ISO-10303-21;
HEADER;
/* Generated by software containing ST-Developer
 * from STEP Tools, Inc. (www.steptools.com) 
 */

FILE_DESCRIPTION(
/* description */ (''),
/* implementation_level */ '2;1');

FILE_NAME(
/* name */ 'Screw.step',
/* time_stamp */ '2026-10-05T15:35:09-07:00',
/* author */ (''),
/* organization */ (''),
/* preprocessor_version */ 'ST-DEVELOPER v20.2',
/* originating_system */ 'Autodesk Translation Framework v15.15.0.0',
/* authorisation */ '');

FILE_SCHEMA (('AUTOMOTIVE_DESIGN { 1 0 10303 214 3 1 1 }'));
ENDSEC;

DATA;
#10=MECHANICAL_DESIGN_GEOMETRIC_PRESENTATION_REPRESENTATION('',(#551),#74523);
#53=B_SPLINE_SURFACE_WITH_KNOTS('',3,3,((#69048,#69049,#69050,#69051,#69052,
#69053,#69054,#69055,#69056,#69057,#69058,#69059,#69060,#69061,#69062,#69063,
#69064,#69065,#69066,#69067,#69068,#69069,#69070,#69071,#69072,#69073,#69074,
#69075,#69076,#69077,#69078,#69079,#69080,#69081,#69082,#69083,#69084,#69085,
#69086,#69087,#69088,#69089,#69090,#69091,#69092,#69093,#69094,#69095,#69096,
#69097,#69098,#69099,#69100,#69101,#69102,#69103,#69104,#69105,#69106,#69107,
#69108,#69109,#69110,#69111,#69112,#69113,#69114,#69115,#69116,#69117,#69118,
#69119,#69120,#69121,#69122,#69123,#69124,#69125,#69126,#69127,#69128,#69129,
#69130,#69131,#69132,#69133,#69134,#69135,#69136,#69137,#69138,#69139,#69140,
#69141,#69142,#69143,#69144,#69145,#69146,#69147,#69148,#69149,#69150,#69151,
#69152,#69153,#69154,#69155,#69156,#69157,#69158,#69159,#69160,#69161,#69162,
#69163,#69164,#69165,#69166,#69167,#69168,#69169,#69170,#69171,#69172,#69173,
#69174,#69175,#69176,#69177,#69178,#69179,#69180,#69181,#69182,#69183,#69184,
#69185,#69186,#69187,#69188,#69189,#69190,#69191,#69192,#69193,#69194,#69195,
#69196,#69197,#69198,#69199,#69200,#69201,#69202,#69203,#69204,#69205,#69206,
#69207,#69208,#69209,#69210,#69211,#69212,#69213,#69214,#69215,#69216,#69217,
#69218,#69219,#69220,#69221,#69222,#69223,#69224,#69225,#69226,#69227,#69228,
#69229,#69230,#69231,#69232,#69233,#69234,#69235,#69236,#69237,#69238,#69239,
#69240,#69241,#69242,#69243,#69244,#69245,#69246,#69247,#69248,#69249,#69250,
#69251,#69252,#69253,#69254,#69255,#69256,#69257,#69258,#69259,#69260,#69261,
#69262,#69263,#69264,#69265,#69266,#69267,#69268,#69269,#69270,#69271,#69272,
#69273,#69274,#69275,#69276,#69277,#69278,#69279,#69280,#69281,#69282,#69283,
#69284,#69285,#69286,#69287,#69288,#69289,#69290,#69291,#69292,#69293,#69294,
#69295,#69296,#69297,#69298,#69299,#69300,#69301,#69302,#69303,#69304,#69305,
#69306,#69307,#69308,#69309,#69310,#69311,#69312,#69313,#69314,#69315,#69316,
#69317,#69318,#69319,#69320,#69321,#69322,#69323,#69324,#69325,#69326,#69327,
#69328,#69329,#69330,#69331,#69332,#69333,#69334,#69335,#69336,#69337,#69338,
#69339,#69340,#69341,#69342,#69343,#69344,#69345,#69346,#69347,#69348,#69349,
#69350,#69351,#69352,#69353,#69354,#69355,#69356,#69357,#69358,#69359,#69360,
#69361,#69362,#69363,#69364,#69365,#69366,#69367,#69368,#69369,#69370,#69371,
#69372,#69373,#69374,#69375,#69376,#69377,#69378,#69379,#69380,#69381,#69382,
#69383,#69384,#69385,#69386,#69387,#69388,#69389,#69390,#69391,#69392,#69393,
#69394,#69395,#69396,#69397,#69398,#69399,#69400,#69401,#69402,#69403,#69404,
#69405,#69406,#69407,#69408,#69409,#69410,#69411,#69412,#69413,#69414,#69415,
#69416,#69417,#69418,#69419,#69420,#69421,#69422,#69423,#69424,#69425,#69426,
#69427,#69428,#69429,#69430,#69431,#69432,#69433,#69434,#69435,#69436,#69437,
#69438,#69439,#69440,#69441,#69442,#69443,#69444,#69445,#69446,#69447,#69448,
#69449,#69450,#69451,#69452,#69453,#69454,#69455,#69456,#69457,#69458,#69459,
#69460,#69461,#69462,#69463,#69464,#69465,#69466,#69467,#69468,#69469,#69470,
#69471,#69472,#69473,#69474,#69475,#69476,#69477,#69478,#69479,#69480,#69481,
#69482,#69483,#69484,#69485,#69486,#69487,#69488,#69489,#69490,#69491,#69492,
#69493,#69494,#69495,#69496,#69497,#69498,#69499,#69500,#69501,#69502,#69503,
#69504,#69505,#69506,#69507,#69508,#69509,#69510,#69511,#69512,#69513,#69514,
#69515,#69516,#69517,#69518,#69519,#69520,#69521,#69522,#69523,#69524,#69525,
#69526,#69527,#69528,#69529,#69530,#69531,#69532,#69533,#69534,#69535,#69536,
#69537,#69538,#69539,#69540,#69541,#69542,#69543,#69544,#69545,#69546,#69547,
#69548,#69549,#69550,#69551,#69552,#69553,#69554,#69555,#69556,#69557,#69558,
#69559,#69560,#69561,#69562,#69563,#69564,#69565,#69566,#69567,#69568,#69569,
#69570,#69571,#69572,#69573,#69574,#69575,#69576,#69577,#69578,#69579,#69580,
#69581,#69582,#69583,#69584,#69585,#69586,#69587,#69588,#69589,#69590,#69591,
#69592,#69593,#69594,#69595,#69596,#69597,#69598,#69599,#69600,#69601,#69602,
#69603,#69604,#69605,#69606,#69607,#69608,#69609,#69610,#69611,#69612,#69613,
#69614,#69615,#69616,#69617,#69618,#69619,#69620,#69621,#69622,#69623,#69624,
#69625,#69626,#69627,#69628,#69629,#69630,#69631,#69632,#69633,#69634,#69635,
#69636,#69637,#69638,#69639,#69640,#69641,#69642,#69643,#69644,#69645,#69646,
#69647,#69648,#69649,#69650,#69651,#69652,#69653,#69654,#69655,#69656,#69657,
#69658,#69659,#69660,#69661,#69662,#69663,#69664,#69665,#69666,#69667,#69668,
#69669,#69670,#69671,#69672,#69673,#69674,#69675,#69676,#69677,#69678,#69679,
#69680,#69681,#69682,#69683,#69684,#69685,#69686,#69687,#69688,#69689,#69690,
#69691,#69692,#69693,#69694,#69695,#69696,#69697,#69698,#69699,#69700,#69701),
(#69702,#69703,#69704,#69705,#69706,#69707,#69708,#69709,#69710,#69711,
#69712,#69713,#69714,#69715,#69716,#69717,#69718,#69719,#69720,#69721,#69722,
#69723,#69724,#69725,#69726,#69727,#69728,#69729,#69730,#69731,#69732,#69733,
#69734,#69735,#69736,#69737,#69738,#69739,#69740,#69741,#69742,#69743,#69744,
#69745,#69746,#69747,#69748,#69749,#69750,#69751,#69752,#69753,#69754,#69755,
#69756,#69757,#69758,#69759,#69760,#69761,#69762,#69763,#69764,#69765,#69766,
#69767,#69768,#69769,#69770,#69771,#69772,#69773,#69774,#69775,#69776,#69777,
#69778,#69779,#69780,#69781,#69782,#69783,#69784,#69785,#69786,#69787,#69788,
#69789,#69790,#69791,#69792,#69793,#69794,#69795,#69796,#69797,#69798,#69799,
#69800,#69801,#69802,#69803,#69804,#69805,#69806,#69807,#69808,#69809,#69810,
#69811,#69812,#69813,#69814,#69815,#69816,#69817,#69818,#69819,#69820,#69821,
#69822,#69823,#69824,#69825,#69826,#69827,#69828,#69829,#69830,#69831,#69832,
#69833,#69834,#69835,#69836,#69837,#69838,#69839,#69840,#69841,#69842,#69843,
#69844,#69845,#69846,#69847,#69848,#69849,#69850,#69851,#69852,#69853,#69854,
#69855,#69856,#69857,#69858,#69859,#69860,#69861,#69862,#69863,#69864,#69865,
#69866,#69867,#69868,#69869,#69870,#69871,#69872,#69873,#69874,#69875,#69876,
#69877,#69878,#69879,#69880,#69881,#69882,#69883,#69884,#69885,#69886,#69887,
#69888,#69889,#69890,#69891,#69892,#69893,#69894,#69895,#69896,#69897,#69898,
#69899,#69900,#69901,#69902,#69903,#69904,#69905,#69906,#69907,#69908,#69909,
#69910,#69911,#69912,#69913,#69914,#69915,#69916,#69917,#69918,#69919,#69920,
#69921,#69922,#69923,#69924,#69925,#69926,#69927,#69928,#69929,#69930,#69931,
#69932,#69933,#69934,#69935,#69936,#69937,#69938,#69939,#69940,#69941,#69942,
#69943,#69944,#69945,#69946,#69947,#69948,#69949,#69950,#69951,#69952,#69953,
#69954,#69955,#69956,#69957,#69958,#69959,#69960,#69961,#69962,#69963,#69964,
#69965,#69966,#69967,#69968,#69969,#69970,#69971,#69972,#69973,#69974,#69975,
#69976,#69977,#69978,#69979,#69980,#69981,#69982,#69983,#69984,#69985,#69986,
#69987,#69988,#69989,#69990,#69991,#69992,#69993,#69994,#69995,#69996,#69997,
#69998,#69999,#70000,#70001,#70002,#70003,#70004,#70005,#70006,#70007,#70008,
#70009,#70010,#70011,#70012,#70013,#70014,#70015,#70016,#70017,#70018,#70019,
#70020,#70021,#70022,#70023,#70024,#70025,#70026,#70027,#70028,#70029,#70030,
#70031,#70032,#70033,#70034,#70035,#70036,#70037,#70038,#70039,#70040,#70041,
#70042,#70043,#70044,#70045,#70046,#70047,#70048,#70049,#70050,#70051,#70052,
#70053,#70054,#70055,#70056,#70057,#70058,#70059,#70060,#70061,#70062,#70063,
#70064,#70065,#70066,#70067,#70068,#70069,#70070,#70071,#70072,#70073,#70074,
#70075,#70076,#70077,#70078,#70079,#70080,#70081,#70082,#70083,#70084,#70085,
#70086,#70087,#70088,#70089,#70090,#70091,#70092,#70093,#70094,#70095,#70096,
#70097,#70098,#70099,#70100,#70101,#70102,#70103,#70104,#70105,#70106,#70107,
#70108,#70109,#70110,#70111,#70112,#70113,#70114,#70115,#70116,#70117,#70118,
#70119,#70120,#70121,#70122,#70123,#70124,#70125,#70126,#70127,#70128,#70129,
#70130,#70131,#70132,#70133,#70134,#70135,#70136,#70137,#70138,#70139,#70140,
#70141,#70142,#70143,#70144,#70145,#70146,#70147,#70148,#70149,#70150,#70151,
#70152,#70153,#70154,#70155,#70156,#70157,#70158,#70159,#70160,#70161,#70162,
#70163,#70164,#70165,#70166,#70167,#70168,#70169,#70170,#70171,#70172,#70173,
#70174,#70175,#70176,#70177,#70178,#70179,#70180,#70181,#70182,#70183,#70184,
#70185,#70186,#70187,#70188,#70189,#70190,#70191,#70192,#70193,#70194,#70195,
#70196,#70197,#70198,#70199,#70200,#70201,#70202,#70203,#70204,#70205,#70206,
#70207,#70208,#70209,#70210,#70211,#70212,#70213,#70214,#70215,#70216,#70217,
#70218,#70219,#70220,#70221,#70222,#70223,#70224,#70225,#70226,#70227,#70228,
#70229,#70230,#70231,#70232,#70233,#70234,#70235,#70236,#70237,#70238,#70239,
#70240,#70241,#70242,#70243,#70244,#70245,#70246,#70247,#70248,#70249,#70250,
#70251,#70252,#70253,#70254,#70255,#70256,#70257,#70258,#70259,#70260,#70261,
#70262,#70263,#70264,#70265,#70266,#70267,#70268,#70269,#70270,#70271,#70272,
#70273,#70274,#70275,#70276,#70277,#70278,#70279,#70280,#70281,#70282,#70283,
#70284,#70285,#70286,#70287,#70288,#70289,#70290,#70291,#70292,#70293,#70294,
#70295,#70296,#70297,#70298,#70299,#70300,#70301,#70302,#70303,#70304,#70305,
#70306,#70307,#70308,#70309,#70310,#70311,#70312,#70313,#70314,#70315,#70316,
#70317,#70318,#70319,#70320,#70321,#70322,#70323,#70324,#70325,#70326,#70327,
#70328,#70329,#70330,#70331,#70332,#70333,#70334,#70335,#70336,#70337,#70338,
#70339,#70340,#70341,#70342,#70343,#70344,#70345,#70346,#70347,#70348,#70349,
#70350,#70351,#70352,#70353,#70354,#70355),(#70356,#70357,#70358,#70359,
#70360,#70361,#70362,#70363,#70364,#70365,#70366,#70367,#70368,#70369,#70370,
#70371,#70372,#70373,#70374,#70375,#70376,#70377,#70378,#70379,#70380,#70381,
#70382,#70383,#70384,#70385,#70386,#70387,#70388,#70389,#70390,#70391,#70392,
#70393,#70394,#70395,#70396,#70397,#70398,#70399,#70400,#70401,#70402,#70403,
#70404,#70405,#70406,#70407,#70408,#70409,#70410,#70411,#70412,#70413,#70414,
#70415,#70416,#70417,#70418,#70419,#70420,#70421,#70422,#70423,#70424,#70425,
#70426,#70427,#70428,#70429,#70430,#70431,#70432,#70433,#70434,#70435,#70436,
#70437,#70438,#70439,#70440,#70441,#70442,#70443,#70444,#70445,#70446,#70447,
#70448,#70449,#70450,#70451,#70452,#70453,#70454,#70455,#70456,#70457,#70458,
#70459,#70460,#70461,#70462,#70463,#70464,#70465,#70466,#70467,#70468,#70469,
#70470,#70471,#70472,#70473,#70474,#70475,#70476,#70477,#70478,#70479,#70480,
#70481,#70482,#70483,#70484,#70485,#70486,#70487,#70488,#70489,#70490,#70491,
#70492,#70493,#70494,#70495,#70496,#70497,#70498,#70499,#70500,#70501,#70502,
#70503,#70504,#70505,#70506,#70507,#70508,#70509,#70510,#70511,#70512,#70513,
#70514,#70515,#70516,#70517,#70518,#70519,#70520,#70521,#70522,#70523,#70524,
#70525,#70526,#70527,#70528,#70529,#70530,#70531,#70532,#70533,#70534,#70535,
#70536,#70537,#70538,#70539,#70540,#70541,#70542,#70543,#70544,#70545,#70546,
#70547,#70548,#70549,#70550,#70551,#70552,#70553,#70554,#70555,#70556,#70557,
#70558,#70559,#70560,#70561,#70562,#70563,#70564,#70565,#70566,#70567,#70568,
#70569,#70570,#70571,#70572,#70573,#70574,#70575,#70576,#70577,#70578,#70579,
#70580,#70581,#70582,#70583,#70584,#70585,#70586,#70587,#70588,#70589,#70590,
#70591,#70592,#70593,#70594,#70595,#70596,#70597,#70598,#70599,#70600,#70601,
#70602,#70603,#70604,#70605,#70606,#70607,#70608,#70609,#70610,#70611,#70612,
#70613,#70614,#70615,#70616,#70617,#70618,#70619,#70620,#70621,#70622,#70623,
#70624,#70625,#70626,#70627,#70628,#70629,#70630,#70631,#70632,#70633,#70634,
#70635,#70636,#70637,#70638,#70639,#70640,#70641,#70642,#70643,#70644,#70645,
#70646,#70647,#70648,#70649,#70650,#70651,#70652,#70653,#70654,#70655,#70656,
#70657,#70658,#70659,#70660,#70661,#70662,#70663,#70664,#70665,#70666,#70667,
#70668,#70669,#70670,#70671,#70672,#70673,#70674,#70675,#70676,#70677,#70678,
#70679,#70680,#70681,#70682,#70683,#70684,#70685,#70686,#70687,#70688,#70689,
#70690,#70691,#70692,#70693,#70694,#70695,#70696,#70697,#70698,#70699,#70700,
#70701,#70702,#70703,#70704,#70705,#70706,#70707,#70708,#70709,#70710,#70711,
#70712,#70713,#70714,#70715,#70716,#70717,#70718,#70719,#70720,#70721,#70722,
#70723,#70724,#70725,#70726,#70727,#70728,#70729,#70730,#70731,#70732,#70733,
#70734,#70735,#70736,#70737,#70738,#70739,#70740,#70741,#70742,#70743,#70744,
#70745,#70746,#70747,#70748,#70749,#70750,#70751,#70752,#70753,#70754,#70755,
#70756,#70757,#70758,#70759,#70760,#70761,#70762,#70763,#70764,#70765,#70766,
#70767,#70768,#70769,#70770,#70771,#70772,#70773,#70774,#70775,#70776,#70777,
#70778,#70779,#70780,#70781,#70782,#70783,#70784,#70785,#70786,#70787,#70788,
#70789,#70790,#70791,#70792,#70793,#70794,#70795,#70796,#70797,#70798,#70799,
#70800,#70801,#70802,#70803,#70804,#70805,#70806,#70807,#70808,#70809,#70810,
#70811,#70812,#70813,#70814,#70815,#70816,#70817,#70818,#70819,#70820,#70821,
#70822,#70823,#70824,#70825,#70826,#70827,#70828,#70829,#70830,#70831,#70832,
#70833,#70834,#70835,#70836,#70837,#70838,#70839,#70840,#70841,#70842,#70843,
#70844,#70845,#70846,#70847,#70848,#70849,#70850,#70851,#70852,#70853,#70854,
#70855,#70856,#70857,#70858,#70859,#70860,#70861,#70862,#70863,#70864,#70865,
#70866,#70867,#70868,#70869,#70870,#70871,#70872,#70873,#70874,#70875,#70876,
#70877,#70878,#70879,#70880,#70881,#70882,#70883,#70884,#70885,#70886,#70887,
#70888,#70889,#70890,#70891,#70892,#70893,#70894,#70895,#70896,#70897,#70898,
#70899,#70900,#70901,#70902,#70903,#70904,#70905,#70906,#70907,#70908,#70909,
#70910,#70911,#70912,#70913,#70914,#70915,#70916,#70917,#70918,#70919,#70920,
#70921,#70922,#70923,#70924,#70925,#70926,#70927,#70928,#70929,#70930,#70931,
#70932,#70933,#70934,#70935,#70936,#70937,#70938,#70939,#70940,#70941,#70942,
#70943,#70944,#70945,#70946,#70947,#70948,#70949,#70950,#70951,#70952,#70953,
#70954,#70955,#70956,#70957,#70958,#70959,#70960,#70961,#70962,#70963,#70964,
#70965,#70966,#70967,#70968,#70969,#70970,#70971,#70972,#70973,#70974,#70975,
#70976,#70977,#70978,#70979,#70980,#70981,#70982,#70983,#70984,#70985,#70986,
#70987,#70988,#70989,#70990,#70991,#70992,#70993,#70994,#70995,#70996,#70997,
#70998,#70999,#71000,#71001,#71002,#71003,#71004,#71005,#71006,#71007,#71008,
#71009),(#71010,#71011,#71012,#71013,#71014,#71015,#71016,#71017,#71018,
#71019,#71020,#71021,#71022,#71023,#71024,#71025,#71026,#71027,#71028,#71029,
#71030,#71031,#71032,#71033,#71034,#71035,#71036,#71037,#71038,#71039,#71040,
#71041,#71042,#71043,#71044,#71045,#71046,#71047,#71048,#71049,#71050,#71051,
#71052,#71053,#71054,#71055,#71056,#71057,#71058,#71059,#71060,#71061,#71062,
#71063,#71064,#71065,#71066,#71067,#71068,#71069,#71070,#71071,#71072,#71073,
#71074,#71075,#71076,#71077,#71078,#71079,#71080,#71081,#71082,#71083,#71084,
#71085,#71086,#71087,#71088,#71089,#71090,#71091,#71092,#71093,#71094,#71095,
#71096,#71097,#71098,#71099,#71100,#71101,#71102,#71103,#71104,#71105,#71106,
#71107,#71108,#71109,#71110,#71111,#71112,#71113,#71114,#71115,#71116,#71117,
#71118,#71119,#71120,#71121,#71122,#71123,#71124,#71125,#71126,#71127,#71128,
#71129,#71130,#71131,#71132,#71133,#71134,#71135,#71136,#71137,#71138,#71139,
#71140,#71141,#71142,#71143,#71144,#71145,#71146,#71147,#71148,#71149,#71150,
#71151,#71152,#71153,#71154,#71155,#71156,#71157,#71158,#71159,#71160,#71161,
#71162,#71163,#71164,#71165,#71166,#71167,#71168,#71169,#71170,#71171,#71172,
#71173,#71174,#71175,#71176,#71177,#71178,#71179,#71180,#71181,#71182,#71183,
#71184,#71185,#71186,#71187,#71188,#71189,#71190,#71191,#71192,#71193,#71194,
#71195,#71196,#71197,#71198,#71199,#71200,#71201,#71202,#71203,#71204,#71205,
#71206,#71207,#71208,#71209,#71210,#71211,#71212,#71213,#71214,#71215,#71216,
#71217,#71218,#71219,#71220,#71221,#71222,#71223,#71224,#71225,#71226,#71227,
#71228,#71229,#71230,#71231,#71232,#71233,#71234,#71235,#71236,#71237,#71238,
#71239,#71240,#71241,#71242,#71243,#71244,#71245,#71246,#71247,#71248,#71249,
#71250,#71251,#71252,#71253,#71254,#71255,#71256,#71257,#71258,#71259,#71260,
#71261,#71262,#71263,#71264,#71265,#71266,#71267,#71268,#71269,#71270,#71271,
#71272,#71273,#71274,#71275,#71276,#71277,#71278,#71279,#71280,#71281,#71282,
#71283,#71284,#71285,#71286,#71287,#71288,#71289,#71290,#71291,#71292,#71293,
#71294,#71295,#71296,#71297,#71298,#71299,#71300,#71301,#71302,#71303,#71304,
#71305,#71306,#71307,#71308,#71309,#71310,#71311,#71312,#71313,#71314,#71315,
#71316,#71317,#71318,#71319,#71320,#71321,#71322,#71323,#71324,#71325,#71326,
#71327,#71328,#71329,#71330,#71331,#71332,#71333,#71334,#71335,#71336,#71337,
#71338,#71339,#71340,#71341,#71342,#71343,#71344,#71345,#71346,#71347,#71348,
#71349,#71350,#71351,#71352,#71353,#71354,#71355,#71356,#71357,#71358,#71359,
#71360,#71361,#71362,#71363,#71364,#71365,#71366,#71367,#71368,#71369,#71370,
#71371,#71372,#71373,#71374,#71375,#71376,#71377,#71378,#71379,#71380,#71381,
#71382,#71383,#71384,#71385,#71386,#71387,#71388,#71389,#71390,#71391,#71392,
#71393,#71394,#71395,#71396,#71397,#71398,#71399,#71400,#71401,#71402,#71403,
#71404,#71405,#71406,#71407,#71408,#71409,#71410,#71411,#71412,#71413,#71414,
#71415,#71416,#71417,#71418,#71419,#71420,#71421,#71422,#71423,#71424,#71425,
#71426,#71427,#71428,#71429,#71430,#71431,#71432,#71433,#71434,#71435,#71436,
#71437,#71438,#71439,#71440,#71441,#71442,#71443,#71444,#71445,#71446,#71447,
#71448,#71449,#71450,#71451,#71452,#71453,#71454,#71455,#71456,#71457,#71458,
#71459,#71460,#71461,#71462,#71463,#71464,#71465,#71466,#71467,#71468,#71469,
#71470,#71471,#71472,#71473,#71474,#71475,#71476,#71477,#71478,#71479,#71480,
#71481,#71482,#71483,#71484,#71485,#71486,#71487,#71488,#71489,#71490,#71491,
#71492,#71493,#71494,#71495,#71496,#71497,#71498,#71499,#71500,#71501,#71502,
#71503,#71504,#71505,#71506,#71507,#71508,#71509,#71510,#71511,#71512,#71513,
#71514,#71515,#71516,#71517,#71518,#71519,#71520,#71521,#71522,#71523,#71524,
#71525,#71526,#71527,#71528,#71529,#71530,#71531,#71532,#71533,#71534,#71535,
#71536,#71537,#71538,#71539,#71540,#71541,#71542,#71543,#71544,#71545,#71546,
#71547,#71548,#71549,#71550,#71551,#71552,#71553,#71554,#71555,#71556,#71557,
#71558,#71559,#71560,#71561,#71562,#71563,#71564,#71565,#71566,#71567,#71568,
#71569,#71570,#71571,#71572,#71573,#71574,#71575,#71576,#71577,#71578,#71579,
#71580,#71581,#71582,#71583,#71584,#71585,#71586,#71587,#71588,#71589,#71590,
#71591,#71592,#71593,#71594,#71595,#71596,#71597,#71598,#71599,#71600,#71601,
#71602,#71603,#71604,#71605,#71606,#71607,#71608,#71609,#71610,#71611,#71612,
#71613,#71614,#71615,#71616,#71617,#71618,#71619,#71620,#71621,#71622,#71623,
#71624,#71625,#71626,#71627,#71628,#71629,#71630,#71631,#71632,#71633,#71634,
#71635,#71636,#71637,#71638,#71639,#71640,#71641,#71642,#71643,#71644,#71645,
#71646,#71647,#71648,#71649,#71650,#71651,#71652,#71653,#71654,#71655,#71656,
#71657,#71658,#71659,#71660,#71661,#71662,#71663)),.UNSPECIFIED.,.F.,.F.,
 .F.,(4,4),(4,1,1,1,1,1,1,1,1,1,1,1,1,1,1,1,1,1,1,1,1,1,1,1,1,1,1,1,1,1,
1,1,1,1,1,1,1,1,1,1,1,1,1,1,1,1,1,1,1,1,1,1,1,1,1,1,1,1,1,1,1,1,1,1,1,1,
1,1,1,1,1,1,1,1,1,1,1,1,1,1,1,1,1,1,1,1,1,1,1,1,1,1,1,1,1,1,1,1,1,1,1,1,
1,1,1,1,1,1,1,1,1,1,1,1,1,1,1,1,1,1,1,1,1,1,1,1,1,1,1,1,1,1,1,1,1,1,1,1,
1,1,1,1,1,1,1,1,1,1,1,1,1,1,1,1,1,1,1,1,1,1,1,1,1,1,1,1,1,1,1,1,1,1,1,1,
1,1,1,1,1,1,1,1,1,1,1,1,1,1,1,1,1,1,1,1,1,1,1,1,1,1,1,1,1,1,1,1,1,1,1,1,
1,1,1,1,1,1,1,1,1,1,1,1,1,1,1,1,1,1,1,1,1,1,1,1,1,1,1,1,1,1,1,1,1,1,1,1,
1,1,1,1,1,1,1,1,1,1,1,1,1,1,1,1,1,1,1,1,1,1,1,1,1,1,1,1,1,1,1,1,1,1,1,1,
1,1,1,1,1,1,1,1,1,1,1,1,1,1,1,1,1,1,1,1,1,1,1,1,1,1,1,1,1,1,1,1,1,1,1,1,
1,1,1,1,1,1,1,1,1,1,1,1,1,1,1,1,1,1,1,1,1,1,1,1,1,1,1,1,1,1,1,1,1,1,1,1,
1,1,1,1,1,1,1,1,1,1,1,1,1,1,1,1,1,1,1,1,1,1,1,1,1,1,1,1,1,1,1,1,1,1,1,1,
1,1,1,1,1,1,1,1,1,1,1,1,1,1,1,1,1,1,1,1,1,1,1,1,1,1,1,1,1,1,1,1,1,1,1,1,
1,1,1,1,1,1,1,1,1,1,1,1,1,1,1,1,1,1,1,1,1,1,1,1,1,1,1,1,1,1,1,1,1,1,1,1,
1,1,1,1,1,1,1,1,1,1,1,1,1,1,1,1,1,1,1,1,1,1,1,1,1,1,1,1,1,1,1,1,1,1,1,1,
1,1,1,1,1,1,1,1,1,1,1,1,1,1,1,1,1,1,1,1,1,1,1,1,1,1,1,1,1,1,1,1,1,1,1,1,
1,1,1,1,1,1,1,1,1,1,1,1,1,1,1,1,1,1,1,1,1,1,1,1,1,1,1,1,1,1,1,1,1,1,1,1,
1,1,1,1,1,1,1,1,1,1,1,1,1,1,1,1,1,1,1,1,1,1,1,1,1,1,1,1,1,1,1,1,1,1,1,1,
1,1,1,1,1,1,1,1,1,1,1,1,1,1,1,1,1,1,1,1,1,1,1,1,1,1,1,1,1,1,1,1,1,1,1,1,
1,1,1,1,1,1,1,1,1,4),(-0.000582827421712283,0.115703455642263),(8.30590425142668,
8.80541461833274,9.30490636943233,10.3038898716315,11.3028733738307,12.3018568760298,
13.300840378229,14.2998238804282,15.2988073826273,16.2977908848265,17.2967743870256,
18.2957578892248,19.294741391424,20.2937248936231,21.2927083958223,22.2916918980215,
23.2906754002206,24.2896589024198,25.288642404619,26.2876259068181,27.2866094090173,
28.2855929112165,29.2845764134156,30.2835599156148,31.282543417814,32.2815269200131,
33.2805104222123,34.2794939244115,35.2784774266106,36.2774609288098,37.276444431009,
38.2754279332081,39.2744114354073,40.2733949376064,41.2723784398056,42.2713619420048,
43.2703454442039,44.2693289464031,45.2683124486023,46.2672959508014,47.2662794530006,
48.2652629551998,49.2642464573989,50.2632299595981,51.2622134617973,52.2611969639964,
53.2601804661956,54.2591639683948,55.2581474705939,56.2571309727931,57.2561144749923,
58.2550979771914,59.2540814793906,60.2530649815898,61.2520484837889,62.2510319859881,
63.2500154881873,64.2489989903864,65.2479824925856,66.2469659947847,67.2459494969839,
68.2449329991831,69.2439165013822,70.2429000035814,71.2418835057806,72.2408670079797,
73.2398505101789,74.2388340123781,75.2378175145772,76.2368010167764,77.2357845189756,
78.2347680211747,79.2337515233739,80.2327350255731,81.2317185277722,82.2307020299714,
83.2296855321705,84.2286690343697,85.2276525365689,86.226636038768,87.2256195409672,
88.2246030431664,89.2235865453655,90.2225700475647,91.2215535497639,92.220537051963,
93.2195205541622,94.2185040563614,95.2174875585605,96.2164710607597,97.2154545629589,
98.214438065158,99.2134215673572,100.212405069556,101.211388571756,102.210372073955,
103.209355576154,104.208339078353,105.207322580552,106.206306082751,107.205289584951,
108.20427308715,109.203256589349,110.202240091548,111.201223593747,112.200207095946,
113.199190598146,114.198174100345,115.197157602544,116.196141104743,117.195124606942,
118.194108109141,119.193091611341,120.19207511354,121.191058615739,122.190042117938,
123.189025620137,124.188009122336,125.186992624535,126.185976126735,127.184959628934,
128.183943131133,129.182926633332,130.181910135531,131.18089363773,132.17987713993,
133.178860642129,134.177844144328,135.176827646527,136.175811148726,137.174794650925,
138.173778153125,139.172761655324,140.171745157523,141.170728659722,142.169712161921,
143.16869566412,144.16767916632,145.166662668519,146.165646170718,147.164629672917,
148.163613175116,149.162596677315,150.161580179515,151.160563681714,152.159547183913,
153.158530686112,154.157514188311,155.15649769051,156.15548119271,157.154464694909,
158.153448197108,159.152431699307,160.151415201506,161.150398703705,162.149382205905,
163.148365708104,164.147349210303,165.146332712502,166.145316214701,167.1442997169,
168.1432832191,169.142266721299,170.141250223498,171.140233725697,172.139217227896,
173.138200730095,174.137184232295,175.136167734494,176.135151236693,177.134134738892,
178.133118241091,179.13210174329,180.13108524549,181.130068747689,182.129052249888,
183.128035752087,184.127019254286,185.126002756485,186.124986258685,187.123969760884,
188.122953263083,189.121936765282,190.120920267481,191.11990376968,192.11888727188,
193.117870774079,194.116854276278,195.115837778477,196.114821280676,197.113804782875,
198.112788285075,199.111771787274,200.110755289473,201.109738791672,202.108722293871,
203.10770579607,204.10668929827,205.105672800469,206.104656302668,207.103639804867,
208.102623307066,209.101606809265,210.100590311465,211.099573813664,212.098557315863,
213.097540818062,214.096524320261,215.09550782246,216.09449132466,217.093474826859,
218.092458329058,219.091441831257,220.090425333456,221.089408835655,222.088392337855,
223.087375840054,224.086359342253,225.085342844452,226.084326346651,227.08330984885,
228.08229335105,229.081276853249,230.080260355448,231.079243857647,232.078227359846,
233.077210862045,234.076194364245,235.075177866444,236.074161368643,237.073144870842,
238.072128373041,239.07111187524,240.070095377439,241.069078879639,242.068062381838,
243.067045884037,244.066029386236,245.065012888435,246.063996390634,247.062979892834,
248.061963395033,249.060946897232,250.059930399431,251.05891390163,252.057897403829,
253.056880906029,254.055864408228,255.054847910427,256.053831412626,257.052814914825,
258.051798417024,259.050781919224,260.049765421423,261.048748923622,262.047732425821,
263.04671592802,264.045699430219,265.044682932419,266.043666434618,267.042649936817,
268.041633439016,269.040616941215,270.039600443414,271.038583945614,272.037567447813,
273.036550950012,274.035534452211,275.03451795441,276.033501456609,277.032484958809,
278.031468461008,279.030451963207,280.029435465406,281.028418967605,282.027402469804,
283.026385972004,284.025369474203,285.024352976402,286.023336478601,287.0223199808,
288.021303482999,289.020286985199,290.019270487398,291.018253989597,292.017237491796,
293.016220993995,294.015204496194,295.014187998394,296.013171500593,297.012155002792,
298.011138504991,299.01012200719,300.009105509389,301.008089011589,302.007072513788,
303.006056015987,304.005039518186,305.004023020385,306.003006522584,307.001990024784,
308.000973526983,308.999957029182,309.998940531381,310.99792403358,311.996907535779,
312.995891037979,313.994874540178,314.993858042377,315.992841544576,316.991825046775,
317.990808548974,318.989792051174,319.988775553373,320.987759055572,321.986742557771,
322.98572605997,323.984709562169,324.983693064369,325.982676566568,326.981660068767,
327.980643570966,328.979627073165,329.978610575364,330.977594077564,331.976577579763,
332.975561081962,333.974544584161,334.97352808636,335.972511588559,336.971495090759,
337.970478592958,338.969462095157,339.968445597356,340.967429099555,341.966412601754,
342.965396103953,343.964379606153,344.963363108352,345.962346610551,346.96133011275,
347.960313614949,348.959297117148,349.958280619348,350.957264121547,351.956247623746,
352.955231125945,353.954214628144,354.953198130343,355.952181632543,356.951165134742,
357.950148636941,358.94913213914,359.948115641339,360.947099143538,361.946082645738,
362.945066147937,363.944049650136,364.943033152335,365.942016654534,366.941000156733,
367.939983658933,368.938967161132,369.937950663331,370.93693416553,371.935917667729,
372.934901169928,373.933884672128,374.932868174327,375.931851676526,376.930835178725,
377.929818680924,378.928802183123,379.927785685323,380.926769187522,381.925752689721,
382.92473619192,383.923719694119,384.922703196318,385.921686698518,386.920670200717,
387.919653702916,388.918637205115,389.917620707314,390.916604209513,391.915587711713,
392.914571213912,393.913554716111,394.91253821831,395.911521720509,396.910505222708,
397.909488724908,398.908472227107,399.907455729306,400.906439231505,401.905422733704,
402.904406235903,403.903389738103,404.902373240302,405.901356742501,406.9003402447,
407.899323746899,408.898307249098,409.897290751298,410.896274253497,411.895257755696,
412.894241257895,413.893224760094,414.892208262293,415.891191764493,416.890175266692,
417.889158768891,418.88814227109,419.887125773289,420.886109275488,421.885092777688,
422.884076279887,423.883059782086,424.882043284285,425.881026786484,426.880010288683,
427.878993790883,428.877977293082,429.876960795281,430.87594429748,431.874927799679,
432.873911301878,433.872894804078,434.871878306277,435.870861808476,436.869845310675,
437.868828812874,438.867812315073,439.866795817273,440.865779319472,441.864762821671,
442.86374632387,443.862729826069,444.861713328268,445.860696830468,446.859680332667,
447.858663834866,448.857647337065,449.856630839264,450.855614341463,451.854597843663,
452.853581345862,453.852564848061,454.85154835026,455.850531852459,456.849515354658,
457.848498856858,458.847482359057,459.846465861256,460.845449363455,461.844432865654,
462.843416367853,463.842399870052,464.841383372252,465.840366874451,466.83935037665,
467.838333878849,468.837317381048,469.836300883247,470.835284385447,471.834267887646,
472.833251389845,473.832234892044,474.831218394243,475.830201896442,476.829185398642,
477.828168900841,478.82715240304,479.826135905239,480.825119407438,481.824102909637,
482.823086411837,483.822069914036,484.821053416235,485.820036918434,486.819020420633,
487.818003922832,488.816987425032,489.815970927231,490.81495442943,491.813937931629,
492.812921433828,493.811904936027,494.810888438227,495.809871940426,496.808855442625,
497.807838944824,498.806822447023,499.805805949222,500.804789451422,501.803772953621,
502.80275645582,503.801739958019,504.800723460218,505.799706962417,506.798690464617,
507.797673966816,508.796657469015,509.795640971214,510.794624473413,511.793607975612,
512.792591477812,513.791574980011,514.79055848221,515.789541984409,516.788525486608,
517.787508988807,518.786492491007,519.785475993206,520.784459495405,521.783442997604,
522.782426499803,523.781410002002,524.780393504201,525.779377006401,526.7783605086,
527.777344010799,528.776327512998,529.775311015197,530.774294517396,531.773278019596,
532.772261521795,533.771245023994,534.770228526193,535.769212028392,536.768195530591,
537.767179032791,538.76616253499,539.765146037189,540.764129539388,541.763113041587,
542.762096543786,543.761080045986,544.760063548185,545.759047050384,546.758030552583,
547.757014054782,548.755997556981,549.754981059181,550.75396456138,551.752948063579,
552.751931565778,553.750915067977,554.749898570176,555.748882072376,556.747865574575,
557.746849076774,558.745832578973,559.744816081172,560.743799583371,561.742783085571,
562.74176658777,563.740750089969,564.739733592168,565.738717094367,566.737700596566,
567.736684098766,568.735667600965,569.734651103164,570.733634605363,571.732618107562,
572.731601609761,573.730585111961,574.72956861416,575.728552116359,576.727535618558,
577.726519120757,578.725502622956,579.724486125156,580.723469627355,581.722453129554,
582.721436631753,583.720420133952,584.719403636151,585.718387138351,586.71737064055,
587.716354142749,588.715337644948,589.714321147147,590.713304649346,591.712288151546,
592.711271653745,593.710255155944,594.709238658143,595.708222160342,596.707205662541,
597.706189164741,598.70517266694,599.704156169139,600.703139671338,601.702123173537,
602.701106675736,603.700090177936,604.699073680135,605.698057182334,606.697040684533,
607.696024186732,608.695007688931,609.693991191131,610.69297469333,611.691958195529,
612.690941697728,613.689925199927,614.688908702126,615.687892204326,616.686875706525,
617.685859208724,618.684842710923,619.683826213122,620.682809715321,621.681793217521,
622.68077671972,623.679760221919,624.678743724118,625.677727226317,626.676710728516,
627.675694230716,628.674677732915,629.673661235114,630.672644737313,631.671628239512,
632.670611741711,633.669595243911,634.66857874611,635.667562248309,636.666545750508,
637.665529252707,638.664512754906,639.663496257106,640.662479759305,641.661463261504,
642.660446763703,643.659430265902,644.658413768101,645.657397270301,646.6563807725,
647.655364274699,648.654347776898,649.653331279097,650.652314781296,651.651298283496,
652.650281785695,653.649265287894,654.648248790093,655.647232292292,656.146724043392,
656.646215794491),.UNSPECIFIED.);
#54=B_SPLINE_SURFACE_WITH_KNOTS('',3,3,((#71773,#71774,#71775,#71776,#71777,
#71778,#71779,#71780,#71781,#71782,#71783,#71784,#71785,#71786,#71787,#71788,
#71789,#71790,#71791,#71792,#71793,#71794,#71795,#71796,#71797,#71798,#71799,
#71800,#71801,#71802,#71803,#71804,#71805,#71806,#71807,#71808,#71809,#71810,
#71811,#71812,#71813,#71814,#71815,#71816,#71817,#71818,#71819,#71820,#71821,
#71822,#71823,#71824,#71825,#71826,#71827,#71828,#71829,#71830,#71831,#71832,
#71833,#71834,#71835,#71836,#71837,#71838,#71839,#71840,#71841,#71842,#71843,
#71844,#71845,#71846,#71847,#71848,#71849,#71850,#71851,#71852,#71853,#71854,
#71855,#71856,#71857,#71858,#71859,#71860,#71861,#71862,#71863,#71864,#71865,
#71866,#71867,#71868,#71869,#71870,#71871,#71872,#71873,#71874,#71875,#71876,
#71877,#71878,#71879,#71880,#71881,#71882,#71883,#71884,#71885,#71886,#71887,
#71888,#71889,#71890,#71891,#71892,#71893,#71894,#71895,#71896,#71897,#71898,
#71899,#71900,#71901,#71902,#71903,#71904,#71905,#71906,#71907,#71908,#71909,
#71910,#71911,#71912,#71913,#71914,#71915,#71916,#71917,#71918,#71919,#71920,
#71921,#71922,#71923,#71924,#71925,#71926,#71927,#71928,#71929,#71930,#71931,
#71932,#71933,#71934,#71935,#71936,#71937,#71938,#71939,#71940,#71941,#71942,
#71943,#71944,#71945,#71946,#71947,#71948,#71949,#71950,#71951,#71952,#71953,
#71954,#71955,#71956,#71957,#71958,#71959,#71960,#71961,#71962,#71963,#71964,
#71965,#71966,#71967,#71968,#71969,#71970,#71971,#71972,#71973,#71974,#71975,
#71976,#71977,#71978,#71979,#71980,#71981,#71982,#71983,#71984,#71985,#71986,
#71987,#71988,#71989,#71990,#71991,#71992,#71993,#71994,#71995,#71996,#71997,
#71998,#71999,#72000,#72001,#72002,#72003,#72004,#72005,#72006,#72007,#72008,
#72009,#72010,#72011,#72012,#72013,#72014,#72015,#72016,#72017,#72018,#72019,
#72020,#72021,#72022,#72023,#72024,#72025,#72026,#72027,#72028,#72029,#72030,
#72031,#72032,#72033,#72034,#72035,#72036,#72037,#72038,#72039,#72040,#72041,
#72042,#72043,#72044,#72045,#72046,#72047,#72048,#72049,#72050,#72051,#72052,
#72053,#72054,#72055,#72056,#72057,#72058,#72059,#72060,#72061,#72062,#72063,
#72064,#72065,#72066,#72067,#72068,#72069,#72070,#72071,#72072,#72073,#72074,
#72075,#72076,#72077,#72078,#72079,#72080,#72081,#72082,#72083,#72084,#72085,
#72086,#72087,#72088,#72089,#72090,#72091,#72092,#72093,#72094,#72095,#72096,
#72097,#72098,#72099,#72100,#72101,#72102,#72103,#72104,#72105,#72106,#72107,
#72108,#72109,#72110,#72111,#72112,#72113,#72114,#72115,#72116,#72117,#72118,
#72119,#72120,#72121,#72122,#72123,#72124,#72125,#72126,#72127,#72128,#72129,
#72130,#72131,#72132,#72133,#72134,#72135,#72136,#72137,#72138,#72139,#72140,
#72141,#72142,#72143,#72144,#72145,#72146,#72147,#72148,#72149,#72150,#72151,
#72152,#72153,#72154,#72155,#72156,#72157,#72158,#72159,#72160,#72161,#72162,
#72163,#72164,#72165,#72166,#72167,#72168,#72169,#72170,#72171,#72172,#72173,
#72174,#72175,#72176,#72177,#72178,#72179,#72180,#72181,#72182,#72183,#72184,
#72185,#72186,#72187,#72188,#72189,#72190,#72191,#72192,#72193,#72194,#72195,
#72196,#72197,#72198,#72199,#72200,#72201,#72202,#72203,#72204,#72205,#72206,
#72207,#72208,#72209,#72210,#72211,#72212,#72213,#72214,#72215,#72216,#72217,
#72218,#72219,#72220,#72221,#72222,#72223,#72224,#72225,#72226,#72227,#72228,
#72229,#72230,#72231,#72232,#72233,#72234,#72235,#72236,#72237,#72238,#72239,
#72240,#72241,#72242,#72243,#72244,#72245,#72246,#72247,#72248,#72249,#72250,
#72251,#72252,#72253,#72254,#72255,#72256,#72257,#72258,#72259,#72260,#72261,
#72262,#72263,#72264,#72265,#72266,#72267,#72268,#72269,#72270,#72271,#72272,
#72273,#72274,#72275,#72276,#72277,#72278,#72279,#72280,#72281,#72282,#72283,
#72284,#72285,#72286,#72287,#72288,#72289,#72290,#72291,#72292,#72293,#72294,
#72295,#72296,#72297,#72298,#72299,#72300,#72301,#72302,#72303,#72304,#72305,
#72306,#72307,#72308,#72309,#72310,#72311,#72312,#72313,#72314,#72315,#72316,
#72317,#72318,#72319,#72320,#72321,#72322,#72323,#72324,#72325,#72326,#72327,
#72328,#72329,#72330,#72331,#72332,#72333,#72334,#72335,#72336,#72337,#72338,
#72339,#72340,#72341,#72342,#72343,#72344,#72345,#72346,#72347,#72348,#72349,
#72350,#72351,#72352,#72353,#72354,#72355,#72356,#72357,#72358,#72359,#72360,
#72361,#72362,#72363,#72364,#72365,#72366,#72367,#72368,#72369,#72370,#72371,
#72372,#72373,#72374,#72375,#72376,#72377,#72378,#72379,#72380,#72381,#72382,
#72383,#72384,#72385,#72386,#72387,#72388,#72389,#72390,#72391,#72392,#72393,
#72394,#72395,#72396,#72397,#72398,#72399,#72400,#72401,#72402,#72403,#72404,
#72405,#72406,#72407,#72408,#72409,#72410,#72411,#72412,#72413,#72414,#72415,
#72416,#72417,#72418,#72419,#72420,#72421,#72422,#72423,#72424,#72425,#72426),
(#72427,#72428,#72429,#72430,#72431,#72432,#72433,#72434,#72435,#72436,
#72437,#72438,#72439,#72440,#72441,#72442,#72443,#72444,#72445,#72446,#72447,
#72448,#72449,#72450,#72451,#72452,#72453,#72454,#72455,#72456,#72457,#72458,
#72459,#72460,#72461,#72462,#72463,#72464,#72465,#72466,#72467,#72468,#72469,
#72470,#72471,#72472,#72473,#72474,#72475,#72476,#72477,#72478,#72479,#72480,
#72481,#72482,#72483,#72484,#72485,#72486,#72487,#72488,#72489,#72490,#72491,
#72492,#72493,#72494,#72495,#72496,#72497,#72498,#72499,#72500,#72501,#72502,
#72503,#72504,#72505,#72506,#72507,#72508,#72509,#72510,#72511,#72512,#72513,
#72514,#72515,#72516,#72517,#72518,#72519,#72520,#72521,#72522,#72523,#72524,
#72525,#72526,#72527,#72528,#72529,#72530,#72531,#72532,#72533,#72534,#72535,
#72536,#72537,#72538,#72539,#72540,#72541,#72542,#72543,#72544,#72545,#72546,
#72547,#72548,#72549,#72550,#72551,#72552,#72553,#72554,#72555,#72556,#72557,
#72558,#72559,#72560,#72561,#72562,#72563,#72564,#72565,#72566,#72567,#72568,
#72569,#72570,#72571,#72572,#72573,#72574,#72575,#72576,#72577,#72578,#72579,
#72580,#72581,#72582,#72583,#72584,#72585,#72586,#72587,#72588,#72589,#72590,
#72591,#72592,#72593,#72594,#72595,#72596,#72597,#72598,#72599,#72600,#72601,
#72602,#72603,#72604,#72605,#72606,#72607,#72608,#72609,#72610,#72611,#72612,
#72613,#72614,#72615,#72616,#72617,#72618,#72619,#72620,#72621,#72622,#72623,
#72624,#72625,#72626,#72627,#72628,#72629,#72630,#72631,#72632,#72633,#72634,
#72635,#72636,#72637,#72638,#72639,#72640,#72641,#72642,#72643,#72644,#72645,
#72646,#72647,#72648,#72649,#72650,#72651,#72652,#72653,#72654,#72655,#72656,
#72657,#72658,#72659,#72660,#72661,#72662,#72663,#72664,#72665,#72666,#72667,
#72668,#72669,#72670,#72671,#72672,#72673,#72674,#72675,#72676,#72677,#72678,
#72679,#72680,#72681,#72682,#72683,#72684,#72685,#72686,#72687,#72688,#72689,
#72690,#72691,#72692,#72693,#72694,#72695,#72696,#72697,#72698,#72699,#72700,
#72701,#72702,#72703,#72704,#72705,#72706,#72707,#72708,#72709,#72710,#72711,
#72712,#72713,#72714,#72715,#72716,#72717,#72718,#72719,#72720,#72721,#72722,
#72723,#72724,#72725,#72726,#72727,#72728,#72729,#72730,#72731,#72732,#72733,
#72734,#72735,#72736,#72737,#72738,#72739,#72740,#72741,#72742,#72743,#72744,
#72745,#72746,#72747,#72748,#72749,#72750,#72751,#72752,#72753,#72754,#72755,
#72756,#72757,#72758,#72759,#72760,#72761,#72762,#72763,#72764,#72765,#72766,
#72767,#72768,#72769,#72770,#72771,#72772,#72773,#72774,#72775,#72776,#72777,
#72778,#72779,#72780,#72781,#72782,#72783,#72784,#72785,#72786,#72787,#72788,
#72789,#72790,#72791,#72792,#72793,#72794,#72795,#72796,#72797,#72798,#72799,
#72800,#72801,#72802,#72803,#72804,#72805,#72806,#72807,#72808,#72809,#72810,
#72811,#72812,#72813,#72814,#72815,#72816,#72817,#72818,#72819,#72820,#72821,
#72822,#72823,#72824,#72825,#72826,#72827,#72828,#72829,#72830,#72831,#72832,
#72833,#72834,#72835,#72836,#72837,#72838,#72839,#72840,#72841,#72842,#72843,
#72844,#72845,#72846,#72847,#72848,#72849,#72850,#72851,#72852,#72853,#72854,
#72855,#72856,#72857,#72858,#72859,#72860,#72861,#72862,#72863,#72864,#72865,
#72866,#72867,#72868,#72869,#72870,#72871,#72872,#72873,#72874,#72875,#72876,
#72877,#72878,#72879,#72880,#72881,#72882,#72883,#72884,#72885,#72886,#72887,
#72888,#72889,#72890,#72891,#72892,#72893,#72894,#72895,#72896,#72897,#72898,
#72899,#72900,#72901,#72902,#72903,#72904,#72905,#72906,#72907,#72908,#72909,
#72910,#72911,#72912,#72913,#72914,#72915,#72916,#72917,#72918,#72919,#72920,
#72921,#72922,#72923,#72924,#72925,#72926,#72927,#72928,#72929,#72930,#72931,
#72932,#72933,#72934,#72935,#72936,#72937,#72938,#72939,#72940,#72941,#72942,
#72943,#72944,#72945,#72946,#72947,#72948,#72949,#72950,#72951,#72952,#72953,
#72954,#72955,#72956,#72957,#72958,#72959,#72960,#72961,#72962,#72963,#72964,
#72965,#72966,#72967,#72968,#72969,#72970,#72971,#72972,#72973,#72974,#72975,
#72976,#72977,#72978,#72979,#72980,#72981,#72982,#72983,#72984,#72985,#72986,
#72987,#72988,#72989,#72990,#72991,#72992,#72993,#72994,#72995,#72996,#72997,
#72998,#72999,#73000,#73001,#73002,#73003,#73004,#73005,#73006,#73007,#73008,
#73009,#73010,#73011,#73012,#73013,#73014,#73015,#73016,#73017,#73018,#73019,
#73020,#73021,#73022,#73023,#73024,#73025,#73026,#73027,#73028,#73029,#73030,
#73031,#73032,#73033,#73034,#73035,#73036,#73037,#73038,#73039,#73040,#73041,
#73042,#73043,#73044,#73045,#73046,#73047,#73048,#73049,#73050,#73051,#73052,
#73053,#73054,#73055,#73056,#73057,#73058,#73059,#73060,#73061,#73062,#73063,
#73064,#73065,#73066,#73067,#73068,#73069,#73070,#73071,#73072,#73073,#73074,
#73075,#73076,#73077,#73078,#73079,#73080),(#73081,#73082,#73083,#73084,
#73085,#73086,#73087,#73088,#73089,#73090,#73091,#73092,#73093,#73094,#73095,
#73096,#73097,#73098,#73099,#73100,#73101,#73102,#73103,#73104,#73105,#73106,
#73107,#73108,#73109,#73110,#73111,#73112,#73113,#73114,#73115,#73116,#73117,
#73118,#73119,#73120,#73121,#73122,#73123,#73124,#73125,#73126,#73127,#73128,
#73129,#73130,#73131,#73132,#73133,#73134,#73135,#73136,#73137,#73138,#73139,
#73140,#73141,#73142,#73143,#73144,#73145,#73146,#73147,#73148,#73149,#73150,
#73151,#73152,#73153,#73154,#73155,#73156,#73157,#73158,#73159,#73160,#73161,
#73162,#73163,#73164,#73165,#73166,#73167,#73168,#73169,#73170,#73171,#73172,
#73173,#73174,#73175,#73176,#73177,#73178,#73179,#73180,#73181,#73182,#73183,
#73184,#73185,#73186,#73187,#73188,#73189,#73190,#73191,#73192,#73193,#73194,
#73195,#73196,#73197,#73198,#73199,#73200,#73201,#73202,#73203,#73204,#73205,
#73206,#73207,#73208,#73209,#73210,#73211,#73212,#73213,#73214,#73215,#73216,
#73217,#73218,#73219,#73220,#73221,#73222,#73223,#73224,#73225,#73226,#73227,
#73228,#73229,#73230,#73231,#73232,#73233,#73234,#73235,#73236,#73237,#73238,
#73239,#73240,#73241,#73242,#73243,#73244,#73245,#73246,#73247,#73248,#73249,
#73250,#73251,#73252,#73253,#73254,#73255,#73256,#73257,#73258,#73259,#73260,
#73261,#73262,#73263,#73264,#73265,#73266,#73267,#73268,#73269,#73270,#73271,
#73272,#73273,#73274,#73275,#73276,#73277,#73278,#73279,#73280,#73281,#73282,
#73283,#73284,#73285,#73286,#73287,#73288,#73289,#73290,#73291,#73292,#73293,
#73294,#73295,#73296,#73297,#73298,#73299,#73300,#73301,#73302,#73303,#73304,
#73305,#73306,#73307,#73308,#73309,#73310,#73311,#73312,#73313,#73314,#73315,
#73316,#73317,#73318,#73319,#73320,#73321,#73322,#73323,#73324,#73325,#73326,
#73327,#73328,#73329,#73330,#73331,#73332,#73333,#73334,#73335,#73336,#73337,
#73338,#73339,#73340,#73341,#73342,#73343,#73344,#73345,#73346,#73347,#73348,
#73349,#73350,#73351,#73352,#73353,#73354,#73355,#73356,#73357,#73358,#73359,
#73360,#73361,#73362,#73363,#73364,#73365,#73366,#73367,#73368,#73369,#73370,
#73371,#73372,#73373,#73374,#73375,#73376,#73377,#73378,#73379,#73380,#73381,
#73382,#73383,#73384,#73385,#73386,#73387,#73388,#73389,#73390,#73391,#73392,
#73393,#73394,#73395,#73396,#73397,#73398,#73399,#73400,#73401,#73402,#73403,
#73404,#73405,#73406,#73407,#73408,#73409,#73410,#73411,#73412,#73413,#73414,
#73415,#73416,#73417,#73418,#73419,#73420,#73421,#73422,#73423,#73424,#73425,
#73426,#73427,#73428,#73429,#73430,#73431,#73432,#73433,#73434,#73435,#73436,
#73437,#73438,#73439,#73440,#73441,#73442,#73443,#73444,#73445,#73446,#73447,
#73448,#73449,#73450,#73451,#73452,#73453,#73454,#73455,#73456,#73457,#73458,
#73459,#73460,#73461,#73462,#73463,#73464,#73465,#73466,#73467,#73468,#73469,
#73470,#73471,#73472,#73473,#73474,#73475,#73476,#73477,#73478,#73479,#73480,
#73481,#73482,#73483,#73484,#73485,#73486,#73487,#73488,#73489,#73490,#73491,
#73492,#73493,#73494,#73495,#73496,#73497,#73498,#73499,#73500,#73501,#73502,
#73503,#73504,#73505,#73506,#73507,#73508,#73509,#73510,#73511,#73512,#73513,
#73514,#73515,#73516,#73517,#73518,#73519,#73520,#73521,#73522,#73523,#73524,
#73525,#73526,#73527,#73528,#73529,#73530,#73531,#73532,#73533,#73534,#73535,
#73536,#73537,#73538,#73539,#73540,#73541,#73542,#73543,#73544,#73545,#73546,
#73547,#73548,#73549,#73550,#73551,#73552,#73553,#73554,#73555,#73556,#73557,
#73558,#73559,#73560,#73561,#73562,#73563,#73564,#73565,#73566,#73567,#73568,
#73569,#73570,#73571,#73572,#73573,#73574,#73575,#73576,#73577,#73578,#73579,
#73580,#73581,#73582,#73583,#73584,#73585,#73586,#73587,#73588,#73589,#73590,
#73591,#73592,#73593,#73594,#73595,#73596,#73597,#73598,#73599,#73600,#73601,
#73602,#73603,#73604,#73605,#73606,#73607,#73608,#73609,#73610,#73611,#73612,
#73613,#73614,#73615,#73616,#73617,#73618,#73619,#73620,#73621,#73622,#73623,
#73624,#73625,#73626,#73627,#73628,#73629,#73630,#73631,#73632,#73633,#73634,
#73635,#73636,#73637,#73638,#73639,#73640,#73641,#73642,#73643,#73644,#73645,
#73646,#73647,#73648,#73649,#73650,#73651,#73652,#73653,#73654,#73655,#73656,
#73657,#73658,#73659,#73660,#73661,#73662,#73663,#73664,#73665,#73666,#73667,
#73668,#73669,#73670,#73671,#73672,#73673,#73674,#73675,#73676,#73677,#73678,
#73679,#73680,#73681,#73682,#73683,#73684,#73685,#73686,#73687,#73688,#73689,
#73690,#73691,#73692,#73693,#73694,#73695,#73696,#73697,#73698,#73699,#73700,
#73701,#73702,#73703,#73704,#73705,#73706,#73707,#73708,#73709,#73710,#73711,
#73712,#73713,#73714,#73715,#73716,#73717,#73718,#73719,#73720,#73721,#73722,
#73723,#73724,#73725,#73726,#73727,#73728,#73729,#73730,#73731,#73732,#73733,
#73734),(#73735,#73736,#73737,#73738,#73739,#73740,#73741,#73742,#73743,
#73744,#73745,#73746,#73747,#73748,#73749,#73750,#73751,#73752,#73753,#73754,
#73755,#73756,#73757,#73758,#73759,#73760,#73761,#73762,#73763,#73764,#73765,
#73766,#73767,#73768,#73769,#73770,#73771,#73772,#73773,#73774,#73775,#73776,
#73777,#73778,#73779,#73780,#73781,#73782,#73783,#73784,#73785,#73786,#73787,
#73788,#73789,#73790,#73791,#73792,#73793,#73794,#73795,#73796,#73797,#73798,
#73799,#73800,#73801,#73802,#73803,#73804,#73805,#73806,#73807,#73808,#73809,
#73810,#73811,#73812,#73813,#73814,#73815,#73816,#73817,#73818,#73819,#73820,
#73821,#73822,#73823,#73824,#73825,#73826,#73827,#73828,#73829,#73830,#73831,
#73832,#73833,#73834,#73835,#73836,#73837,#73838,#73839,#73840,#73841,#73842,
#73843,#73844,#73845,#73846,#73847,#73848,#73849,#73850,#73851,#73852,#73853,
#73854,#73855,#73856,#73857,#73858,#73859,#73860,#73861,#73862,#73863,#73864,
#73865,#73866,#73867,#73868,#73869,#73870,#73871,#73872,#73873,#73874,#73875,
#73876,#73877,#73878,#73879,#73880,#73881,#73882,#73883,#73884,#73885,#73886,
#73887,#73888,#73889,#73890,#73891,#73892,#73893,#73894,#73895,#73896,#73897,
#73898,#73899,#73900,#73901,#73902,#73903,#73904,#73905,#73906,#73907,#73908,
#73909,#73910,#73911,#73912,#73913,#73914,#73915,#73916,#73917,#73918,#73919,
#73920,#73921,#73922,#73923,#73924,#73925,#73926,#73927,#73928,#73929,#73930,
#73931,#73932,#73933,#73934,#73935,#73936,#73937,#73938,#73939,#73940,#73941,
#73942,#73943,#73944,#73945,#73946,#73947,#73948,#73949,#73950,#73951,#73952,
#73953,#73954,#73955,#73956,#73957,#73958,#73959,#73960,#73961,#73962,#73963,
#73964,#73965,#73966,#73967,#73968,#73969,#73970,#73971,#73972,#73973,#73974,
#73975,#73976,#73977,#73978,#73979,#73980,#73981,#73982,#73983,#73984,#73985,
#73986,#73987,#73988,#73989,#73990,#73991,#73992,#73993,#73994,#73995,#73996,
#73997,#73998,#73999,#74000,#74001,#74002,#74003,#74004,#74005,#74006,#74007,
#74008,#74009,#74010,#74011,#74012,#74013,#74014,#74015,#74016,#74017,#74018,
#74019,#74020,#74021,#74022,#74023,#74024,#74025,#74026,#74027,#74028,#74029,
#74030,#74031,#74032,#74033,#74034,#74035,#74036,#74037,#74038,#74039,#74040,
#74041,#74042,#74043,#74044,#74045,#74046,#74047,#74048,#74049,#74050,#74051,
#74052,#74053,#74054,#74055,#74056,#74057,#74058,#74059,#74060,#74061,#74062,
#74063,#74064,#74065,#74066,#74067,#74068,#74069,#74070,#74071,#74072,#74073,
#74074,#74075,#74076,#74077,#74078,#74079,#74080,#74081,#74082,#74083,#74084,
#74085,#74086,#74087,#74088,#74089,#74090,#74091,#74092,#74093,#74094,#74095,
#74096,#74097,#74098,#74099,#74100,#74101,#74102,#74103,#74104,#74105,#74106,
#74107,#74108,#74109,#74110,#74111,#74112,#74113,#74114,#74115,#74116,#74117,
#74118,#74119,#74120,#74121,#74122,#74123,#74124,#74125,#74126,#74127,#74128,
#74129,#74130,#74131,#74132,#74133,#74134,#74135,#74136,#74137,#74138,#74139,
#74140,#74141,#74142,#74143,#74144,#74145,#74146,#74147,#74148,#74149,#74150,
#74151,#74152,#74153,#74154,#74155,#74156,#74157,#74158,#74159,#74160,#74161,
#74162,#74163,#74164,#74165,#74166,#74167,#74168,#74169,#74170,#74171,#74172,
#74173,#74174,#74175,#74176,#74177,#74178,#74179,#74180,#74181,#74182,#74183,
#74184,#74185,#74186,#74187,#74188,#74189,#74190,#74191,#74192,#74193,#74194,
#74195,#74196,#74197,#74198,#74199,#74200,#74201,#74202,#74203,#74204,#74205,
#74206,#74207,#74208,#74209,#74210,#74211,#74212,#74213,#74214,#74215,#74216,
#74217,#74218,#74219,#74220,#74221,#74222,#74223,#74224,#74225,#74226,#74227,
#74228,#74229,#74230,#74231,#74232,#74233,#74234,#74235,#74236,#74237,#74238,
#74239,#74240,#74241,#74242,#74243,#74244,#74245,#74246,#74247,#74248,#74249,
#74250,#74251,#74252,#74253,#74254,#74255,#74256,#74257,#74258,#74259,#74260,
#74261,#74262,#74263,#74264,#74265,#74266,#74267,#74268,#74269,#74270,#74271,
#74272,#74273,#74274,#74275,#74276,#74277,#74278,#74279,#74280,#74281,#74282,
#74283,#74284,#74285,#74286,#74287,#74288,#74289,#74290,#74291,#74292,#74293,
#74294,#74295,#74296,#74297,#74298,#74299,#74300,#74301,#74302,#74303,#74304,
#74305,#74306,#74307,#74308,#74309,#74310,#74311,#74312,#74313,#74314,#74315,
#74316,#74317,#74318,#74319,#74320,#74321,#74322,#74323,#74324,#74325,#74326,
#74327,#74328,#74329,#74330,#74331,#74332,#74333,#74334,#74335,#74336,#74337,
#74338,#74339,#74340,#74341,#74342,#74343,#74344,#74345,#74346,#74347,#74348,
#74349,#74350,#74351,#74352,#74353,#74354,#74355,#74356,#74357,#74358,#74359,
#74360,#74361,#74362,#74363,#74364,#74365,#74366,#74367,#74368,#74369,#74370,
#74371,#74372,#74373,#74374,#74375,#74376,#74377,#74378,#74379,#74380,#74381,
#74382,#74383,#74384,#74385,#74386,#74387,#74388)),.UNSPECIFIED.,.F.,.F.,
 .F.,(4,4),(4,1,1,1,1,1,1,1,1,1,1,1,1,1,1,1,1,1,1,1,1,1,1,1,1,1,1,1,1,1,
1,1,1,1,1,1,1,1,1,1,1,1,1,1,1,1,1,1,1,1,1,1,1,1,1,1,1,1,1,1,1,1,1,1,1,1,
1,1,1,1,1,1,1,1,1,1,1,1,1,1,1,1,1,1,1,1,1,1,1,1,1,1,1,1,1,1,1,1,1,1,1,1,
1,1,1,1,1,1,1,1,1,1,1,1,1,1,1,1,1,1,1,1,1,1,1,1,1,1,1,1,1,1,1,1,1,1,1,1,
1,1,1,1,1,1,1,1,1,1,1,1,1,1,1,1,1,1,1,1,1,1,1,1,1,1,1,1,1,1,1,1,1,1,1,1,
1,1,1,1,1,1,1,1,1,1,1,1,1,1,1,1,1,1,1,1,1,1,1,1,1,1,1,1,1,1,1,1,1,1,1,1,
1,1,1,1,1,1,1,1,1,1,1,1,1,1,1,1,1,1,1,1,1,1,1,1,1,1,1,1,1,1,1,1,1,1,1,1,
1,1,1,1,1,1,1,1,1,1,1,1,1,1,1,1,1,1,1,1,1,1,1,1,1,1,1,1,1,1,1,1,1,1,1,1,
1,1,1,1,1,1,1,1,1,1,1,1,1,1,1,1,1,1,1,1,1,1,1,1,1,1,1,1,1,1,1,1,1,1,1,1,
1,1,1,1,1,1,1,1,1,1,1,1,1,1,1,1,1,1,1,1,1,1,1,1,1,1,1,1,1,1,1,1,1,1,1,1,
1,1,1,1,1,1,1,1,1,1,1,1,1,1,1,1,1,1,1,1,1,1,1,1,1,1,1,1,1,1,1,1,1,1,1,1,
1,1,1,1,1,1,1,1,1,1,1,1,1,1,1,1,1,1,1,1,1,1,1,1,1,1,1,1,1,1,1,1,1,1,1,1,
1,1,1,1,1,1,1,1,1,1,1,1,1,1,1,1,1,1,1,1,1,1,1,1,1,1,1,1,1,1,1,1,1,1,1,1,
1,1,1,1,1,1,1,1,1,1,1,1,1,1,1,1,1,1,1,1,1,1,1,1,1,1,1,1,1,1,1,1,1,1,1,1,
1,1,1,1,1,1,1,1,1,1,1,1,1,1,1,1,1,1,1,1,1,1,1,1,1,1,1,1,1,1,1,1,1,1,1,1,
1,1,1,1,1,1,1,1,1,1,1,1,1,1,1,1,1,1,1,1,1,1,1,1,1,1,1,1,1,1,1,1,1,1,1,1,
1,1,1,1,1,1,1,1,1,1,1,1,1,1,1,1,1,1,1,1,1,1,1,1,1,1,1,1,1,1,1,1,1,1,1,1,
1,1,1,1,1,1,1,1,1,1,1,1,1,1,1,1,1,1,1,1,1,1,1,1,1,1,1,1,1,1,1,1,1,1,1,1,
1,1,1,1,1,1,1,1,1,4),(-0.000422349804609623,0.11588507652678),(11.6153159187298,
12.114913270212,12.6144050213115,13.6133885235107,14.6123720257099,15.611355527909,
16.6103390301082,17.6093225323074,18.6083060345065,19.6072895367057,20.6062730389049,
21.605256541104,22.6042400433032,23.6032235455024,24.6022070477015,25.6011905499007,
26.6001740520998,27.599157554299,28.5981410564982,29.5971245586973,30.5961080608965,
31.5950915630957,32.5940750652948,33.593058567494,34.5920420696932,35.5910255718923,
36.5900090740915,37.5889925762907,38.5879760784898,39.586959580689,40.5859430828882,
41.5849265850873,42.5839100872865,43.5828935894856,44.5818770916848,45.580860593884,
46.5798440960831,47.5788275982823,48.5778111004815,49.5767946026806,50.5757781048798,
51.574761607079,52.5737451092781,53.5727286114773,54.5717121136765,55.5706956158756,
56.5696791180748,57.5686626202739,58.5676461224731,59.5666296246723,60.5656131268714,
61.5645966290706,62.5635801312698,63.5625636334689,64.5615471356681,65.5605306378673,
66.5595141400664,67.5584976422656,68.5574811444648,69.5564646466639,70.5554481488631,
71.5544316510623,72.5534151532614,73.5523986554606,74.5513821576597,75.5503656598589,
76.5493491620581,77.5483326642572,78.5473161664564,79.5462996686556,80.5452831708547,
81.5442666730539,82.5432501752531,83.5422336774522,84.5412171796514,85.5402006818506,
86.5391841840497,87.5381676862489,88.5371511884481,89.5361346906472,90.5351181928464,
91.5341016950455,92.5330851972447,93.5320686994439,94.531052201643,95.5300357038422,
96.5290192060414,97.5280027082405,98.5269862104397,99.5259697126389,100.524953214838,
101.523936717037,102.522920219236,103.521903721436,104.520887223635,105.519870725834,
106.518854228033,107.517837730232,108.516821232431,109.515804734631,110.51478823683,
111.513771739029,112.512755241228,113.511738743427,114.510722245626,115.509705747826,
116.508689250025,117.507672752224,118.506656254423,119.505639756622,120.504623258821,
121.50360676102,122.50259026322,123.501573765419,124.500557267618,125.499540769817,
126.498524272016,127.497507774215,128.496491276415,129.495474778614,130.494458280813,
131.493441783012,132.492425285211,133.49140878741,134.49039228961,135.489375791809,
136.488359294008,137.487342796207,138.486326298406,139.485309800605,140.484293302805,
141.483276805004,142.482260307203,143.481243809402,144.480227311601,145.4792108138,
146.478194316,147.477177818199,148.476161320398,149.475144822597,150.474128324796,
151.473111826995,152.472095329195,153.471078831394,154.470062333593,155.469045835792,
156.468029337991,157.46701284019,158.46599634239,159.464979844589,160.463963346788,
161.462946848987,162.461930351186,163.460913853385,164.459897355585,165.458880857784,
166.457864359983,167.456847862182,168.455831364381,169.45481486658,170.45379836878,
171.452781870979,172.451765373178,173.450748875377,174.449732377576,175.448715879775,
176.447699381975,177.446682884174,178.445666386373,179.444649888572,180.443633390771,
181.44261689297,182.44160039517,183.440583897369,184.439567399568,185.438550901767,
186.437534403966,187.436517906165,188.435501408365,189.434484910564,190.433468412763,
191.432451914962,192.431435417161,193.43041891936,194.429402421559,195.428385923759,
196.427369425958,197.426352928157,198.425336430356,199.424319932555,200.423303434754,
201.422286936954,202.421270439153,203.420253941352,204.419237443551,205.41822094575,
206.417204447949,207.416187950149,208.415171452348,209.414154954547,210.413138456746,
211.412121958945,212.411105461144,213.410088963344,214.409072465543,215.408055967742,
216.407039469941,217.40602297214,218.405006474339,219.403989976539,220.402973478738,
221.401956980937,222.400940483136,223.399923985335,224.398907487534,225.397890989734,
226.396874491933,227.395857994132,228.394841496331,229.39382499853,230.392808500729,
231.391792002929,232.390775505128,233.389759007327,234.388742509526,235.387726011725,
236.386709513924,237.385693016124,238.384676518323,239.383660020522,240.382643522721,
241.38162702492,242.380610527119,243.379594029319,244.378577531518,245.377561033717,
246.376544535916,247.375528038115,248.374511540314,249.373495042514,250.372478544713,
251.371462046912,252.370445549111,253.36942905131,254.368412553509,255.367396055709,
256.366379557908,257.365363060107,258.364346562306,259.363330064505,260.362313566704,
261.361297068904,262.360280571103,263.359264073302,264.358247575501,265.3572310777,
266.356214579899,267.355198082099,268.354181584298,269.353165086497,270.352148588696,
271.351132090895,272.350115593094,273.349099095293,274.348082597493,275.347066099692,
276.346049601891,277.34503310409,278.344016606289,279.343000108488,280.341983610688,
281.340967112887,282.339950615086,283.338934117285,284.337917619484,285.336901121683,
286.335884623883,287.334868126082,288.333851628281,289.33283513048,290.331818632679,
291.330802134878,292.329785637078,293.328769139277,294.327752641476,295.326736143675,
296.325719645874,297.324703148073,298.323686650273,299.322670152472,300.321653654671,
301.32063715687,302.319620659069,303.318604161268,304.317587663468,305.316571165667,
306.315554667866,307.314538170065,308.313521672264,309.312505174463,310.311488676663,
311.310472178862,312.309455681061,313.30843918326,314.307422685459,315.306406187658,
316.305389689858,317.304373192057,318.303356694256,319.302340196455,320.301323698654,
321.300307200853,322.299290703053,323.298274205252,324.297257707451,325.29624120965,
326.295224711849,327.294208214048,328.293191716248,329.292175218447,330.291158720646,
331.290142222845,332.289125725044,333.288109227243,334.287092729443,335.286076231642,
336.285059733841,337.28404323604,338.283026738239,339.282010240438,340.280993742638,
341.279977244837,342.278960747036,343.277944249235,344.276927751434,345.275911253633,
346.274894755833,347.273878258032,348.272861760231,349.27184526243,350.270828764629,
351.269812266828,352.268795769027,353.267779271227,354.266762773426,355.265746275625,
356.264729777824,357.263713280023,358.262696782222,359.261680284422,360.260663786621,
361.25964728882,362.258630791019,363.257614293218,364.256597795417,365.255581297617,
366.254564799816,367.253548302015,368.252531804214,369.251515306413,370.250498808612,
371.249482310812,372.248465813011,373.24744931521,374.246432817409,375.245416319608,
376.244399821807,377.243383324007,378.242366826206,379.241350328405,380.240333830604,
381.239317332803,382.238300835002,383.237284337202,384.236267839401,385.2352513416,
386.234234843799,387.233218345998,388.232201848197,389.231185350397,390.230168852596,
391.229152354795,392.228135856994,393.227119359193,394.226102861392,395.225086363592,
396.224069865791,397.22305336799,398.222036870189,399.221020372388,400.220003874587,
401.218987376787,402.217970878986,403.216954381185,404.215937883384,405.214921385583,
406.213904887782,407.212888389982,408.211871892181,409.21085539438,410.209838896579,
411.208822398778,412.207805900977,413.206789403177,414.205772905376,415.204756407575,
416.203739909774,417.202723411973,418.201706914172,419.200690416372,420.199673918571,
421.19865742077,422.197640922969,423.196624425168,424.195607927367,425.194591429567,
426.193574931766,427.192558433965,428.191541936164,429.190525438363,430.189508940562,
431.188492442761,432.187475944961,433.18645944716,434.185442949359,435.184426451558,
436.183409953757,437.182393455956,438.181376958156,439.180360460355,440.179343962554,
441.178327464753,442.177310966952,443.176294469151,444.175277971351,445.17426147355,
446.173244975749,447.172228477948,448.171211980147,449.170195482346,450.169178984546,
451.168162486745,452.167145988944,453.166129491143,454.165112993342,455.164096495541,
456.163079997741,457.16206349994,458.161047002139,459.160030504338,460.159014006537,
461.157997508736,462.156981010936,463.155964513135,464.154948015334,465.153931517533,
466.152915019732,467.151898521931,468.150882024131,469.14986552633,470.148849028529,
471.147832530728,472.146816032927,473.145799535126,474.144783037326,475.143766539525,
476.142750041724,477.141733543923,478.140717046122,479.139700548321,480.138684050521,
481.13766755272,482.136651054919,483.135634557118,484.134618059317,485.133601561516,
486.132585063716,487.131568565915,488.130552068114,489.129535570313,490.128519072512,
491.127502574711,492.126486076911,493.12546957911,494.124453081309,495.123436583508,
496.122420085707,497.121403587906,498.120387090106,499.119370592305,500.118354094504,
501.117337596703,502.116321098902,503.115304601101,504.114288103301,505.1132716055,
506.112255107699,507.111238609898,508.110222112097,509.109205614296,510.108189116495,
511.107172618695,512.106156120894,513.105139623093,514.104123125292,515.103106627491,
516.102090129691,517.10107363189,518.100057134089,519.099040636288,520.098024138487,
521.097007640686,522.095991142886,523.094974645085,524.093958147284,525.092941649483,
526.091925151682,527.090908653881,528.08989215608,529.08887565828,530.087859160479,
531.086842662678,532.085826164877,533.084809667076,534.083793169275,535.082776671475,
536.081760173674,537.080743675873,538.079727178072,539.078710680271,540.07769418247,
541.07667768467,542.075661186869,543.074644689068,544.073628191267,545.072611693466,
546.071595195665,547.070578697865,548.069562200064,549.068545702263,550.067529204462,
551.066512706661,552.06549620886,553.06447971106,554.063463213259,555.062446715458,
556.061430217657,557.060413719856,558.059397222055,559.058380724255,560.057364226454,
561.056347728653,562.055331230852,563.054314733051,564.05329823525,565.05228173745,
566.051265239649,567.050248741848,568.049232244047,569.048215746246,570.047199248445,
571.046182750645,572.045166252844,573.044149755043,574.043133257242,575.042116759441,
576.04110026164,577.040083763839,578.039067266039,579.038050768238,580.037034270437,
581.036017772636,582.035001274835,583.033984777034,584.032968279234,585.031951781433,
586.030935283632,587.029918785831,588.02890228803,589.027885790229,590.026869292429,
591.025852794628,592.024836296827,593.023819799026,594.022803301225,595.021786803424,
596.020770305624,597.019753807823,598.018737310022,599.017720812221,600.01670431442,
601.015687816619,602.014671318819,603.013654821018,604.012638323217,605.011621825416,
606.010605327615,607.009588829814,608.008572332014,609.007555834213,610.006539336412,
611.005522838611,612.00450634081,613.003489843009,614.002473345209,615.001456847408,
616.000440349607,616.999423851806,617.998407354005,618.997390856204,619.996374358404,
620.995357860603,621.994341362802,622.993324865001,623.9923083672,624.991291869399,
625.990275371599,626.989258873798,627.988242375997,628.987225878196,629.986209380395,
630.985192882594,631.984176384793,632.983159886993,633.982143389192,634.981126891391,
635.98011039359,636.979093895789,637.978077397988,638.977060900188,639.976044402387,
640.975027904586,641.974011406785,642.972994908984,643.971978411183,644.970961913383,
645.969945415582,646.968928917781,647.96791241998,648.966895922179,649.965879424378,
650.964862926578,651.963846428777,652.962829930976,653.961813433175,654.960796935374,
655.959780437573,656.958763939773,657.957747441972,658.956730944171,659.456222695271,
659.95571444637),.UNSPECIFIED.);
#102=B_SPLINE_CURVE_WITH_KNOTS('',3,(#7985,#7986,#7987,#7988,#7989,#7990,
#7991,#7992,#7993,#7994,#7995,#7996,#7997,#7998,#7999,#8000,#8001,#8002,
#8003,#8004,#8005,#8006,#8007,#8008,#8009,#8010,#8011,#8012,#8013,#8014,
#8015,#8016,#8017,#8018,#8019,#8020,#8021,#8022,#8023,#8024,#8025,#8026,
#8027,#8028,#8029,#8030,#8031,#8032,#8033,#8034,#8035,#8036,#8037,#8038,
#8039,#8040,#8041,#8042,#8043,#8044,#8045,#8046,#8047,#8048,#8049,#8050,
#8051,#8052,#8053,#8054,#8055,#8056,#8057,#8058,#8059,#8060,#8061,#8062,
#8063),.UNSPECIFIED.,.F.,.F.,(4,3,3,3,3,3,3,3,3,3,3,3,3,3,3,3,3,3,3,3,3,
3,3,3,3,3,4),(-4.09254174883824,-3.99593400879665,-3.91583620996095,-3.83583142168521,
-3.75590227074564,-3.67603144249985,-3.59620166787706,-3.51638411379587,
-3.43656945874385,-3.35674210619879,-3.27688645516505,-3.19694352471772,
-3.11695137442049,-3.03684665274117,-2.99695050659749,-2.91844690823361,
-2.84003781292725,-2.76170459532558,-2.68342871723619,-2.60518487891826,
-2.52695644729207,-2.44872674633489,-2.37047909991097,-2.29215102845281,
-2.21378107360774,-2.13529261516942,-2.07059485109299),.UNSPECIFIED.);
#103=B_SPLINE_CURVE_WITH_KNOTS('',3,(#8067,#8068,#8069,#8070,#8071,#8072,
#8073,#8074,#8075,#8076,#8077,#8078,#8079,#8080,#8081,#8082,#8083,#8084,
#8085,#8086,#8087,#8088,#8089,#8090,#8091,#8092,#8093,#8094,#8095,#8096,
#8097,#8098,#8099,#8100,#8101,#8102,#8103,#8104,#8105,#8106,#8107,#8108,
#8109),.UNSPECIFIED.,.F.,.F.,(4,3,3,3,3,3,3,3,3,3,3,3,3,3,4),(0.,0.0935644284073191,
0.18729632151828,0.281031513390348,0.374648205279863,0.467922871498954,
0.499491751099595,0.579460878581141,0.659419998763359,0.739384630924569,
0.819398568293176,0.899442161096395,0.979559995621145,0.998983502199193,
1.11885509353981),.UNSPECIFIED.);
#104=B_SPLINE_CURVE_WITH_KNOTS('',3,(#8111,#8112,#8113,#8114,#8115,#8116,
#8117,#8118,#8119,#8120,#8121,#8122,#8123,#8124,#8125,#8126,#8127,#8128,
#8129,#8130,#8131,#8132,#8133,#8134,#8135,#8136,#8137,#8138,#8139,#8140,
#8141,#8142,#8143,#8144,#8145,#8146,#8147,#8148,#8149,#8150,#8151,#8152,
#8153,#8154,#8155,#8156,#8157,#8158,#8159,#8160,#8161,#8162,#8163,#8164,
#8165,#8166,#8167,#8168,#8169,#8170,#8171,#8172,#8173,#8174,#8175,#8176,
#8177,#8178,#8179,#8180,#8181,#8182,#8183,#8184,#8185,#8186,#8187,#8188,
#8189,#8190,#8191,#8192,#8193,#8194,#8195,#8196,#8197,#8198,#8199,#8200,
#8201,#8202,#8203,#8204,#8205,#8206,#8207,#8208,#8209,#8210,#8211,#8212,
#8213,#8214,#8215,#8216,#8217,#8218,#8219,#8220,#8221,#8222,#8223,#8224,
#8225,#8226,#8227,#8228,#8229,#8230,#8231,#8232,#8233,#8234,#8235,#8236,
#8237,#8238,#8239,#8240,#8241,#8242,#8243,#8244,#8245,#8246,#8247,#8248,
#8249,#8250,#8251,#8252,#8253,#8254,#8255,#8256,#8257,#8258,#8259,#8260,
#8261,#8262,#8263,#8264,#8265,#8266,#8267,#8268,#8269,#8270,#8271,#8272,
#8273,#8274,#8275,#8276,#8277,#8278,#8279,#8280,#8281,#8282,#8283,#8284,
#8285,#8286,#8287,#8288,#8289,#8290,#8291,#8292,#8293,#8294,#8295,#8296,
#8297,#8298,#8299,#8300,#8301,#8302,#8303,#8304,#8305,#8306,#8307,#8308,
#8309,#8310,#8311,#8312,#8313,#8314,#8315,#8316,#8317,#8318,#8319,#8320,
#8321,#8322,#8323,#8324,#8325,#8326,#8327,#8328,#8329,#8330,#8331,#8332,
#8333,#8334,#8335,#8336,#8337,#8338,#8339,#8340,#8341,#8342,#8343,#8344,
#8345,#8346,#8347,#8348,#8349,#8350,#8351,#8352,#8353,#8354),
 .UNSPECIFIED.,.F.,.F.,(4,3,3,3,3,3,3,3,3,3,3,3,3,3,3,3,3,3,3,3,3,3,3,3,
3,3,3,3,3,3,3,3,3,3,3,3,3,3,3,3,3,3,3,3,3,3,3,3,3,3,3,3,3,3,3,3,3,3,3,3,
3,3,3,3,3,3,3,3,3,3,3,3,3,3,3,3,3,3,3,3,3,4),(1.11885509365731,1.19890888242023,
1.27890195600316,1.35885150057562,1.43878687530592,1.51871708466099,1.59865764641746,
1.67862408146344,1.7586825532862,1.8387877251625,1.91902312927819,1.99796700439835,
2.07727102857866,2.15647325956687,2.23559184022159,2.31464483775223,2.39365026085368,
2.47263617598548,2.55161468675081,2.63060203582996,2.70961446936347,2.78871342568456,
2.86785984415472,2.94712339981395,2.9969505065975,3.07705312821031,3.1570619066815,
3.23699421838189,3.31686738045404,3.39669866385784,3.47651649014003,3.55633064916348,
3.63615673738681,3.71601035527486,3.7959500957172,3.87593839432808,3.95603826859724,
3.99593400879665,4.07599768389782,4.15596874230769,4.23586459502544,4.31570259458817,
4.39550004816396,4.47528616612706,4.55506994268505,4.63486700962401,4.714693003592,
4.79460740114907,4.87457161678181,4.95464958904228,4.99491751099581,5.07478899813074,
5.15456501822308,5.23426318727578,5.3139010592233,5.39349613977932,5.47307716442314,
5.55265417799236,5.63224298538747,5.71185939566583,5.79156324137428,5.87131604149074,
5.95118306081602,5.99390101319496,6.07389207539437,6.15378892336041,6.23360904990546,
6.31336988767804,6.39308882254675,6.47279463932957,6.55249701617323,6.63221165251339,
6.71195425208848,6.79178420386357,6.87166325245412,6.9516556575512,6.99288451539411,
7.08126525070436,7.16930398900817,7.25712468236554,7.3445872388794,7.40204018941607),
 .UNSPECIFIED.);
#105=B_SPLINE_CURVE_WITH_KNOTS('',3,(#8356,#8357,#8358,#8359,#8360,#8361,
#8362,#8363,#8364,#8365),.UNSPECIFIED.,.F.,.F.,(4,1,1,1,1,1,1,4),(7.40204040071942,
7.99186801759328,8.99085151979246,9.98983502199165,10.9888185241908,11.98780202639,
12.9867855285892,13.6852257078989),.UNSPECIFIED.);
#106=B_SPLINE_CURVE_WITH_KNOTS('',3,(#8367,#8368,#8369,#8370,#8371,#8372,
#8373,#8374,#8375,#8376,#8377,#8378,#8379,#8380,#8381,#8382,#8383,#8384,
#8385,#8386,#8387,#8388,#8389,#8390,#8391,#8392,#8393,#8394,#8395,#8396,
#8397,#8398,#8399,#8400,#8401,#8402,#8403,#8404,#8405,#8406,#8407,#8408,
#8409,#8410,#8411,#8412,#8413,#8414,#8415,#8416,#8417,#8418,#8419,#8420,
#8421,#8422,#8423,#8424,#8425,#8426,#8427,#8428,#8429,#8430,#8431,#8432,
#8433,#8434,#8435,#8436,#8437,#8438,#8439,#8440,#8441,#8442,#8443,#8444,
#8445,#8446,#8447,#8448,#8449,#8450,#8451,#8452,#8453,#8454,#8455,#8456,
#8457,#8458,#8459,#8460,#8461,#8462,#8463,#8464,#8465,#8466,#8467,#8468,
#8469,#8470,#8471,#8472,#8473,#8474,#8475,#8476,#8477,#8478,#8479,#8480,
#8481,#8482,#8483,#8484,#8485,#8486,#8487,#8488,#8489,#8490,#8491,#8492,
#8493,#8494,#8495,#8496,#8497,#8498,#8499,#8500,#8501,#8502,#8503,#8504,
#8505,#8506,#8507,#8508,#8509,#8510,#8511,#8512,#8513,#8514,#8515,#8516,
#8517,#8518,#8519,#8520,#8521,#8522,#8523,#8524,#8525,#8526,#8527,#8528,
#8529,#8530,#8531,#8532,#8533,#8534,#8535,#8536,#8537,#8538,#8539,#8540,
#8541,#8542,#8543,#8544,#8545,#8546,#8547,#8548,#8549,#8550,#8551,#8552,
#8553,#8554,#8555,#8556,#8557,#8558,#8559,#8560,#8561,#8562,#8563,#8564,
#8565,#8566,#8567,#8568,#8569,#8570,#8571,#8572,#8573,#8574,#8575,#8576,
#8577,#8578,#8579,#8580,#8581,#8582,#8583,#8584,#8585,#8586,#8587,#8588,
#8589,#8590,#8591,#8592,#8593,#8594,#8595,#8596,#8597,#8598,#8599,#8600,
#8601,#8602,#8603,#8604,#8605,#8606,#8607,#8608,#8609,#8610,#8611,#8612,
#8613),.UNSPECIFIED.,.F.,.F.,(4,3,3,3,3,3,3,3,3,3,3,3,3,3,3,3,3,3,3,3,3,
3,3,3,3,3,3,3,3,3,3,3,3,3,3,3,3,3,3,3,3,3,3,3,3,3,3,3,3,3,3,3,3,3,3,3,3,
3,3,3,3,3,3,3,3,3,3,3,3,3,3,3,3,3,3,3,3,3,3,3,3,3,4),(13.6852258923761,
13.7811381458858,13.8778420020683,13.9753729543055,13.9857690307884,14.0657337088802,
14.1456040124813,14.2253974614937,14.3051315153514,14.3848235864942,14.4645025074165,
14.5441779714702,14.623865701738,14.7035814256359,14.7833846844125,14.8632371039494,
14.9432032095308,14.9847525329875,15.0647176274353,15.1445883524893,15.2243822276137,
15.3041167118116,15.3838092170969,15.4634885764725,15.5431644816131,15.6228526552282,
15.7025688243615,15.7823725290164,15.8622253954616,15.9421919457269,15.9837360351867,
16.063700994944,16.143571584348,16.2233653230009,16.3030996700424,16.3827920376221,
16.4624712589146,16.5421470257523,16.6218350609649,16.7015510917162,16.7813546587208,
16.8612073877251,16.9411738020618,16.9827195373858,17.0626844575672,17.1425550065156,
17.2223487038769,17.3020830088335,17.3817753335765,17.4614545110396,17.5411302334353,
17.6208182236289,17.7005342088199,17.7803377296644,17.8601904120997,17.9401567796245,
17.981703039585,18.0616680202291,18.1415386304136,18.2213323897207,18.3010667572697,
18.3807591451903,18.4604383865057,18.5401141731666,18.619802227984,18.6995182781033,
18.7793218640147,18.8591746116927,18.9391410441751,18.9806865417842,19.0604936907362,
19.1402065480529,19.2198427864482,19.299420016977,19.3830438917397,19.4625667314659,
19.542087693453,19.6216226370564,19.7011874271912,19.7808399463116,19.860543555116,
19.9403569248264,19.9684110150785),.UNSPECIFIED.);
#107=B_SPLINE_CURVE_WITH_KNOTS('',3,(#8615,#8616,#8617,#8618,#8619,#8620,
#8621,#8622,#8623,#8624,#8625,#8626),.UNSPECIFIED.,.F.,.F.,(4,2,1,1,1,1,
1,1,4),(19.9684110150785,19.9796700439833,20.9786535461825,21.9776370483816,
22.9766205505808,23.9756040527799,24.9745875549791,25.9735710571782,26.2515921566761),
 .UNSPECIFIED.);
#108=B_SPLINE_CURVE_WITH_KNOTS('',3,(#8628,#8629,#8630,#8631,#8632,#8633,
#8634,#8635,#8636,#8637,#8638,#8639,#8640,#8641,#8642,#8643,#8644,#8645,
#8646,#8647,#8648,#8649,#8650,#8651,#8652,#8653,#8654,#8655,#8656,#8657,
#8658,#8659,#8660,#8661,#8662,#8663,#8664,#8665,#8666,#8667,#8668,#8669,
#8670,#8671,#8672,#8673,#8674,#8675,#8676,#8677,#8678,#8679,#8680,#8681,
#8682,#8683,#8684,#8685,#8686,#8687,#8688,#8689,#8690,#8691,#8692,#8693,
#8694,#8695,#8696,#8697,#8698,#8699,#8700,#8701,#8702,#8703,#8704,#8705,
#8706,#8707,#8708,#8709,#8710,#8711,#8712,#8713,#8714,#8715,#8716,#8717,
#8718,#8719,#8720,#8721,#8722,#8723,#8724,#8725,#8726,#8727,#8728,#8729,
#8730,#8731,#8732,#8733,#8734,#8735,#8736,#8737,#8738,#8739,#8740,#8741,
#8742,#8743,#8744,#8745,#8746,#8747,#8748,#8749,#8750,#8751,#8752,#8753,
#8754,#8755,#8756,#8757,#8758,#8759,#8760,#8761,#8762,#8763,#8764,#8765,
#8766,#8767,#8768,#8769,#8770,#8771,#8772,#8773,#8774,#8775,#8776,#8777,
#8778,#8779,#8780,#8781,#8782,#8783,#8784,#8785,#8786,#8787,#8788,#8789,
#8790,#8791,#8792,#8793,#8794,#8795,#8796,#8797,#8798,#8799,#8800,#8801,
#8802,#8803,#8804,#8805,#8806,#8807,#8808,#8809,#8810,#8811,#8812,#8813,
#8814,#8815,#8816,#8817,#8818,#8819,#8820,#8821,#8822,#8823,#8824,#8825,
#8826,#8827,#8828,#8829,#8830,#8831,#8832,#8833,#8834,#8835,#8836,#8837,
#8838,#8839,#8840,#8841,#8842,#8843,#8844,#8845,#8846,#8847,#8848,#8849,
#8850,#8851,#8852,#8853,#8854,#8855,#8856,#8857,#8858,#8859,#8860,#8861,
#8862,#8863,#8864,#8865,#8866,#8867,#8868,#8869,#8870,#8871),
 .UNSPECIFIED.,.F.,.F.,(4,3,3,3,3,3,3,3,3,3,3,3,3,3,3,3,3,3,3,3,3,3,3,3,
3,3,3,3,3,3,3,3,3,3,3,3,3,3,3,3,3,3,3,3,3,3,3,3,3,3,3,3,3,3,3,3,3,3,3,3,
3,3,3,3,3,3,3,3,3,3,3,3,3,3,3,3,3,3,3,3,3,4),(26.2515963222581,26.3306329510203,
26.4108731520649,26.4898610484131,26.5688492534367,26.647854020369,26.7290291551211,
26.8081567839455,26.8903556716614,26.9725545593774,27.0525195182439,27.1323901064284,
27.2121838435362,27.2919181887089,27.3716105540985,27.4512897727228,27.5309655365955,
27.6106535685474,27.6903695957433,27.7701731587582,27.8500258835208,27.9299922932555,
27.9715380615766,28.0515030203413,28.1313736084233,28.2111673454273,28.2909016904953,
28.3705940557787,28.4502732742969,28.5299490380631,28.6096370699079,28.6893530969969,
28.7691566599045,28.8490093845593,28.9289757941872,28.9705215637758,29.0504865225538,
29.130357110649,29.2101508476663,29.2898851927477,29.3695775580446,29.4492567765757,
29.5289325403545,29.6086205722123,29.6883365993133,29.7681401622332,29.8479928869009,
29.9279592965406,29.969505065975,30.0494700247739,30.1293406128902,30.2091343499289,
30.2888686950319,30.3685610603512,30.4482402789046,30.5279160427061,30.6076040745864,
30.6873201017102,30.7671236646531,30.8469763893435,30.9269427990063,30.9684885681741,
31.0484535269574,31.1283241150579,31.2081178520804,31.2878521971676,31.3675445624705,
31.4472237810075,31.5268995447925,31.6065875766561,31.6863036037632,31.7661071666897,
31.8459598913635,31.9259263010099,31.9674720703733,32.0493953620172,32.1312078546291,
32.212922693681,32.2945286616084,32.3760709623789,32.4575526442695,32.5347816294377),
 .UNSPECIFIED.);
#109=B_SPLINE_CURVE_WITH_KNOTS('',3,(#8873,#8874,#8875,#8876,#8877,#8878,
#8879,#8880,#8881,#8882),.UNSPECIFIED.,.F.,.F.,(4,1,1,1,1,1,1,4),(32.5347869710949,
32.9664555725725,33.9654390747716,34.9644225769708,35.9634060791699,36.9623895813691,
37.9613730835682,38.8179669366173),.UNSPECIFIED.);
#110=B_SPLINE_CURVE_WITH_KNOTS('',3,(#8884,#8885,#8886,#8887,#8888,#8889,
#8890,#8891,#8892,#8893,#8894),.UNSPECIFIED.,.F.,.F.,(4,1,1,1,1,1,1,1,4),
(38.8179669366173,38.9603565857674,39.9593400879665,40.9583235901657,41.9573070923649,
42.9562905945641,43.9552740967633,44.9542575989625,45.101152243797),
 .UNSPECIFIED.);
#111=B_SPLINE_CURVE_WITH_KNOTS('',3,(#8896,#8897,#8898,#8899,#8900,#8901,
#8902,#8903,#8904,#8905),.UNSPECIFIED.,.F.,.F.,(4,1,1,1,1,1,1,4),(45.101152243797,
45.9532411011617,46.9522246033608,47.95120810556,48.9501916077592,49.9491751099583,
50.9481586121575,51.3843324992521),.UNSPECIFIED.);
#112=B_SPLINE_CURVE_WITH_KNOTS('',3,(#8907,#8908,#8909,#8910,#8911,#8912,
#8913,#8914,#8915,#8916,#8917,#8918,#8919,#8920,#8921,#8922,#8923,#8924,
#8925,#8926,#8927,#8928,#8929,#8930,#8931,#8932,#8933,#8934,#8935,#8936,
#8937,#8938,#8939,#8940,#8941,#8942,#8943,#8944,#8945,#8946,#8947,#8948,
#8949,#8950,#8951,#8952,#8953,#8954,#8955,#8956,#8957,#8958,#8959,#8960,
#8961,#8962,#8963,#8964,#8965,#8966,#8967,#8968,#8969,#8970,#8971,#8972,
#8973,#8974,#8975,#8976,#8977,#8978,#8979,#8980,#8981,#8982,#8983,#8984,
#8985,#8986,#8987,#8988,#8989,#8990,#8991,#8992,#8993,#8994,#8995,#8996,
#8997,#8998,#8999,#9000,#9001,#9002,#9003,#9004,#9005,#9006,#9007,#9008,
#9009,#9010,#9011,#9012,#9013,#9014,#9015,#9016,#9017,#9018,#9019,#9020,
#9021,#9022,#9023,#9024,#9025,#9026,#9027,#9028,#9029,#9030,#9031,#9032,
#9033,#9034,#9035,#9036,#9037,#9038,#9039,#9040,#9041,#9042,#9043,#9044,
#9045,#9046,#9047,#9048,#9049,#9050,#9051,#9052,#9053,#9054,#9055,#9056,
#9057,#9058,#9059,#9060,#9061,#9062,#9063,#9064,#9065,#9066,#9067,#9068,
#9069,#9070,#9071,#9072,#9073,#9074,#9075,#9076,#9077,#9078,#9079,#9080,
#9081,#9082,#9083,#9084,#9085,#9086,#9087,#9088,#9089,#9090,#9091,#9092,
#9093,#9094,#9095,#9096,#9097,#9098,#9099,#9100,#9101,#9102,#9103,#9104,
#9105,#9106,#9107,#9108,#9109,#9110,#9111,#9112,#9113,#9114,#9115,#9116,
#9117,#9118,#9119,#9120,#9121,#9122,#9123,#9124,#9125,#9126,#9127,#9128,
#9129,#9130,#9131,#9132,#9133,#9134,#9135,#9136,#9137,#9138,#9139,#9140,
#9141,#9142,#9143,#9144,#9145,#9146,#9147,#9148,#9149,#9150,#9151,#9152,
#9153),.UNSPECIFIED.,.F.,.F.,(4,3,3,3,3,3,3,3,3,3,3,3,3,3,3,3,3,3,3,3,3,
3,3,3,3,3,3,3,3,3,3,3,3,3,3,3,3,3,3,3,3,3,3,3,3,3,3,3,3,3,3,3,3,3,3,3,3,
3,3,3,3,3,3,3,3,3,3,3,3,3,3,3,3,3,3,3,3,3,3,3,3,3,4),(51.3843375509764,
51.4659219703665,51.5475504548222,51.6292356660958,51.711051351291,51.7929351797258,
51.8749722248705,51.9471421143566,52.0271070731438,52.1069776612481,52.1867713982747,
52.2665057433655,52.3461981086724,52.4258773272134,52.5055530910026,52.5852411228703,
52.6649571499817,52.744760712912,52.8246134375896,52.90457984724,52.9461256165558,
53.0260905753431,53.1059611634476,53.1857549004743,53.2654892455655,53.3451816108724,
53.4248608294136,53.5045365932028,53.5842246250706,53.6639406521816,53.7437442151119,
53.8235969397897,53.9035633494401,53.9451091187549,54.0250740775424,54.1049446656471,
54.1847384026741,54.2644727477653,54.3441651130724,54.4238443316137,54.503520095403,
54.5832081272712,54.6629241543834,54.7427277173139,54.8225804419923,54.9025468516429,
54.9440926209541,55.0240575797413,55.1039281678459,55.1837219048729,55.2634562499639,
55.3431486152707,55.4228278338118,55.5025035976009,55.5821916294688,55.6619076565804,
55.7417112195109,55.8215639441889,55.9015303538393,55.9430761231532,56.0230410819406,
56.1029116700452,56.1827054070721,56.2624397521628,56.3421321174705,56.4218113360118,
56.501487099801,56.5811751316687,56.6608911587802,56.7406947217107,56.8205474463889,
56.9005138560392,56.9420596253524,57.0213023256814,57.1020798922408,57.1811290941038,
57.2601247624458,57.3390832275544,57.4211931352048,57.5001424786768,57.5791007326911,
57.6581021560049,57.6675228581561),.UNSPECIFIED.);
#113=B_SPLINE_CURVE_WITH_KNOTS('',3,(#9155,#9156,#9157,#9158,#9159,#9160,
#9161,#9162,#9163,#9164,#9165),.UNSPECIFIED.,.F.,.F.,(4,1,1,1,1,1,1,1,4),
(57.6675266605331,57.9410431275516,58.9400266297507,59.9390101319499,60.9379936341491,
61.9369771363482,62.9359606385474,63.9349441407466,63.9507081653357),
 .UNSPECIFIED.);
#114=B_SPLINE_CURVE_WITH_KNOTS('',3,(#9167,#9168,#9169,#9170,#9171,#9172,
#9173,#9174,#9175,#9176,#9177,#9178,#9179,#9180,#9181,#9182,#9183,#9184,
#9185,#9186,#9187,#9188,#9189,#9190,#9191,#9192,#9193,#9194,#9195,#9196,
#9197,#9198,#9199,#9200,#9201,#9202,#9203,#9204,#9205,#9206,#9207,#9208,
#9209,#9210,#9211,#9212,#9213,#9214,#9215,#9216,#9217,#9218,#9219,#9220,
#9221,#9222,#9223,#9224,#9225,#9226,#9227,#9228,#9229,#9230,#9231,#9232,
#9233,#9234,#9235,#9236,#9237,#9238,#9239,#9240,#9241,#9242,#9243,#9244,
#9245,#9246,#9247,#9248,#9249,#9250,#9251,#9252,#9253,#9254,#9255,#9256,
#9257,#9258,#9259,#9260,#9261,#9262,#9263,#9264,#9265,#9266,#9267,#9268,
#9269,#9270,#9271,#9272,#9273,#9274,#9275,#9276,#9277,#9278,#9279,#9280,
#9281,#9282,#9283,#9284,#9285,#9286,#9287,#9288,#9289,#9290,#9291,#9292,
#9293,#9294,#9295,#9296,#9297,#9298,#9299,#9300,#9301,#9302,#9303,#9304,
#9305,#9306,#9307,#9308,#9309,#9310,#9311,#9312,#9313,#9314,#9315,#9316,
#9317,#9318,#9319,#9320,#9321,#9322,#9323,#9324,#9325,#9326,#9327,#9328,
#9329,#9330,#9331,#9332,#9333,#9334,#9335,#9336,#9337,#9338,#9339,#9340,
#9341,#9342,#9343,#9344,#9345,#9346,#9347,#9348,#9349,#9350,#9351,#9352,
#9353,#9354,#9355,#9356,#9357,#9358,#9359,#9360,#9361,#9362,#9363,#9364,
#9365,#9366,#9367,#9368,#9369,#9370,#9371,#9372,#9373,#9374,#9375,#9376,
#9377,#9378,#9379,#9380,#9381,#9382,#9383,#9384,#9385,#9386,#9387,#9388,
#9389,#9390,#9391,#9392,#9393,#9394,#9395,#9396,#9397,#9398,#9399,#9400,
#9401,#9402,#9403,#9404,#9405,#9406,#9407,#9408,#9409,#9410,#9411,#9412,
#9413),.UNSPECIFIED.,.F.,.F.,(4,3,3,3,3,3,3,3,3,3,3,3,3,3,3,3,3,3,3,3,3,
3,3,3,3,3,3,3,3,3,3,3,3,3,3,3,3,3,3,3,3,3,3,3,3,3,3,3,3,3,3,3,3,3,3,3,3,
3,3,3,3,3,3,3,3,3,3,3,3,3,3,3,3,3,3,3,3,3,3,3,3,3,4),(63.9507081653357,
64.0304540093271,64.1101058619716,64.1896814506261,64.2691984406716,64.3522895909558,
64.4317533767242,64.5112157170839,64.5906925209173,64.6701997030615,64.7497948088937,
64.8294415713291,64.9091973059203,64.9339276429458,65.0138926017331,65.0937631898377,
65.1735569268647,65.2532912719556,65.3329836372622,65.4126628558034,65.4923386195927,
65.5720266514604,65.6517426785721,65.7315462415026,65.8113989661805,65.8913653758311,
65.9329111451449,66.0128761039322,66.092746692037,66.1725404290636,66.2522747741544,
66.3319671394608,66.4116463580019,66.4913221217909,66.5710101536589,66.6507261807705,
66.7305297437008,66.8103824683786,66.890348878029,66.9318946473441,67.0118596061315,
67.091730194236,67.1715239312629,67.2512582763545,67.3309506416611,67.4106298602024,
67.4903056239916,67.5699936558595,67.6497096829711,67.7295132459017,67.8093659705799,
67.8893323802304,67.9308781495432,68.0108431083305,68.090713696435,68.1705074334619,
68.250241778553,68.3299341438601,68.4096133624013,68.4892891261903,68.5689771580581,
68.64869318517,68.7284967481004,68.8083494727784,68.888315882429,68.9298616517423,
69.0098266105296,69.089697198634,69.1694909356608,69.2492252807525,69.3289176460595,
69.4085968646007,69.4882726283898,69.5679606602578,69.6476766873696,69.7274802502999,
69.8073329749774,69.8872993846278,69.9288451539415,70.0256929206329,70.1219607775206,
70.2171816476072,70.2338932790561),.UNSPECIFIED.);
#115=B_SPLINE_CURVE_WITH_KNOTS('',3,(#9415,#9416,#9417,#9418,#9419,#9420,
#9421,#9422,#9423,#9424),.UNSPECIFIED.,.F.,.F.,(4,1,1,1,1,1,1,4),(70.2338934725153,
70.9278286561406,71.9268121583398,72.925795660539,73.9247791627382,74.9237626649374,
75.9227461671366,76.5170787796949),.UNSPECIFIED.);
#116=B_SPLINE_CURVE_WITH_KNOTS('',3,(#9426,#9427,#9428,#9429,#9430,#9431,
#9432,#9433,#9434,#9435,#9436,#9437,#9438,#9439,#9440,#9441,#9442,#9443,
#9444,#9445,#9446,#9447,#9448,#9449,#9450,#9451,#9452,#9453,#9454,#9455,
#9456,#9457,#9458,#9459,#9460,#9461,#9462,#9463,#9464,#9465,#9466,#9467,
#9468,#9469,#9470,#9471,#9472,#9473,#9474,#9475,#9476,#9477,#9478,#9479,
#9480,#9481,#9482,#9483,#9484,#9485,#9486,#9487,#9488,#9489,#9490,#9491,
#9492,#9493,#9494,#9495,#9496,#9497,#9498,#9499,#9500,#9501,#9502,#9503,
#9504,#9505,#9506,#9507,#9508,#9509,#9510,#9511,#9512,#9513,#9514,#9515,
#9516,#9517,#9518,#9519,#9520,#9521,#9522,#9523,#9524,#9525,#9526,#9527,
#9528,#9529,#9530,#9531,#9532,#9533,#9534,#9535,#9536,#9537,#9538,#9539,
#9540,#9541,#9542,#9543,#9544,#9545,#9546,#9547,#9548,#9549,#9550,#9551,
#9552,#9553,#9554,#9555,#9556,#9557,#9558,#9559,#9560,#9561,#9562,#9563,
#9564,#9565,#9566,#9567,#9568,#9569,#9570,#9571,#9572,#9573,#9574,#9575,
#9576,#9577,#9578,#9579,#9580,#9581,#9582,#9583,#9584,#9585,#9586,#9587,
#9588,#9589,#9590,#9591,#9592,#9593,#9594,#9595,#9596,#9597,#9598,#9599,
#9600,#9601,#9602,#9603,#9604,#9605,#9606,#9607,#9608,#9609,#9610,#9611,
#9612,#9613,#9614,#9615,#9616,#9617,#9618,#9619,#9620,#9621,#9622,#9623,
#9624,#9625,#9626,#9627,#9628,#9629,#9630,#9631,#9632,#9633,#9634,#9635,
#9636,#9637,#9638,#9639,#9640,#9641,#9642,#9643,#9644,#9645,#9646,#9647,
#9648,#9649,#9650,#9651,#9652,#9653,#9654,#9655,#9656,#9657,#9658,#9659,
#9660,#9661,#9662,#9663,#9664,#9665,#9666,#9667,#9668,#9669,#9670,#9671,
#9672),.UNSPECIFIED.,.F.,.F.,(4,3,3,3,3,3,3,3,3,3,3,3,3,3,3,3,3,3,3,3,3,
3,3,3,3,3,3,3,3,3,3,3,3,3,3,3,3,3,3,3,3,3,3,3,3,3,3,3,3,3,3,3,3,3,3,3,3,
3,3,3,3,3,3,3,3,3,3,3,3,3,3,3,3,3,3,3,3,3,3,3,3,3,4),(76.5170789972737,
76.604724745235,76.6928108189936,76.7811201939996,76.8697456009293,76.9217296693358,
77.0016946281234,77.0815652162282,77.1613589532554,77.2410932983468,77.3207856636539,
77.4004648821953,77.4801406459847,77.5598286778528,77.6395447049645,77.7193482678952,
77.7992009925734,77.8791674022242,77.9207131715349,78.0006781303222,78.0805487184268,
78.1603424554537,78.2400768005447,78.3197691658517,78.3994483843929,78.4791241481821,
78.55881218005,78.6385282071615,78.718331770092,78.7981844947699,78.8781509044204,
78.9196966737341,78.9996616325214,79.0795322206259,79.1593259576527,79.2390603027437,
79.3187526680505,79.3984318865917,79.4781076503808,79.5577956822486,79.63751170936,
79.7173152722904,79.7971679969683,79.8771344066187,79.9186801759332,79.9986451347205,
80.0785157228252,80.158309459852,80.2380438049431,80.31773617025,80.3974153887912,
80.4770911525804,80.5567791844482,80.6364952115598,80.7162987744902,80.7961514991682,
80.8761179088187,80.9176636781324,80.9976286369197,81.0774992250243,81.1572929620511,
81.2370273071422,81.3167196724491,81.3963988909903,81.4760746547794,81.5557626866472,
81.6354787137588,81.7152822766893,81.7951350013672,81.8751014110176,81.9166471803315,
81.9955344657586,82.0743281297056,82.1530465802032,82.2339487685371,82.3125756196587,
82.3911872681938,82.469800214983,82.5524161829559,82.6311178282799,82.7098621033094,
82.7886974136541,82.8002640868745),.UNSPECIFIED.);
#117=B_SPLINE_CURVE_WITH_KNOTS('',3,(#9674,#9675,#9676,#9677,#9678,#9679,
#9680,#9681,#9682,#9683,#9684),.UNSPECIFIED.,.F.,.F.,(4,1,1,1,1,1,1,1,4),
(82.8002640868745,82.9156306825307,83.9146141847298,84.913597686929,85.9125811891282,
86.9115646913274,87.9105481935266,88.9095316957258,89.0834493940541),
 .UNSPECIFIED.);
#118=B_SPLINE_CURVE_WITH_KNOTS('',3,(#9686,#9687,#9688,#9689,#9690,#9691,
#9692,#9693,#9694,#9695,#9696,#9697,#9698,#9699,#9700,#9701,#9702,#9703,
#9704,#9705,#9706,#9707,#9708,#9709,#9710,#9711,#9712,#9713,#9714,#9715,
#9716,#9717,#9718,#9719,#9720,#9721,#9722,#9723,#9724,#9725,#9726,#9727,
#9728,#9729,#9730,#9731,#9732,#9733,#9734,#9735,#9736,#9737,#9738,#9739,
#9740,#9741,#9742,#9743,#9744,#9745,#9746,#9747,#9748,#9749,#9750,#9751,
#9752,#9753,#9754,#9755,#9756,#9757,#9758,#9759,#9760,#9761,#9762,#9763,
#9764,#9765,#9766,#9767,#9768,#9769,#9770,#9771,#9772,#9773,#9774,#9775,
#9776,#9777,#9778,#9779,#9780,#9781,#9782,#9783,#9784,#9785,#9786,#9787,
#9788,#9789,#9790,#9791,#9792,#9793,#9794,#9795,#9796,#9797,#9798,#9799,
#9800,#9801,#9802,#9803,#9804,#9805,#9806,#9807,#9808,#9809,#9810,#9811,
#9812,#9813,#9814,#9815,#9816,#9817,#9818,#9819,#9820,#9821,#9822,#9823,
#9824,#9825,#9826,#9827,#9828,#9829,#9830,#9831,#9832,#9833,#9834,#9835,
#9836,#9837,#9838,#9839,#9840,#9841,#9842,#9843,#9844,#9845,#9846,#9847,
#9848,#9849,#9850,#9851,#9852,#9853,#9854,#9855,#9856,#9857,#9858,#9859,
#9860,#9861,#9862,#9863,#9864,#9865,#9866,#9867,#9868,#9869,#9870,#9871,
#9872,#9873,#9874,#9875,#9876,#9877,#9878,#9879,#9880,#9881,#9882,#9883,
#9884,#9885,#9886,#9887,#9888,#9889,#9890,#9891,#9892,#9893,#9894,#9895,
#9896,#9897,#9898,#9899,#9900,#9901,#9902,#9903,#9904,#9905,#9906,#9907,
#9908,#9909,#9910,#9911,#9912,#9913,#9914,#9915,#9916,#9917,#9918,#9919,
#9920,#9921,#9922,#9923,#9924,#9925,#9926,#9927,#9928,#9929,#9930,#9931,
#9932),.UNSPECIFIED.,.F.,.F.,(4,3,3,3,3,3,3,3,3,3,3,3,3,3,3,3,3,3,3,3,3,
3,3,3,3,3,3,3,3,3,3,3,3,3,3,3,3,3,3,3,3,3,3,3,3,3,3,3,3,3,3,3,3,3,3,3,3,
3,3,3,3,3,3,3,3,3,3,3,3,3,3,3,3,3,3,3,3,3,3,3,3,3,4),(89.0834493940541,
89.162104822173,89.24069050899,89.319224841056,89.3977345280541,89.4762339591774,
89.5547396989003,89.6332683149672,89.7118787705787,89.7905353918081,89.8693023315089,
89.9085151979249,89.9884801567122,90.0683507448169,90.1481444818438,90.2278788269349,
90.3075711922417,90.387250410783,90.4669261745722,90.54661420644,90.6263302335514,
90.7061337964818,90.7859865211597,90.8659529308102,90.9074987001241,90.9874636589114,
91.067334247016,91.1471279840428,91.2268623291339,91.306554694441,91.3862339129823,
91.4659096767714,91.5455977086393,91.6253137357504,91.7051172986808,91.7849700233589,
91.8649364330094,91.9064822023232,91.9864471611105,92.0663177492151,92.1461114862419,
92.2258458313331,92.3055381966401,92.3852174151813,92.4648931789704,92.5445812108382,
92.6242972379498,92.7041008008802,92.7839535255579,92.8639199352083,92.9054657045224,
92.9854306633098,93.0653012514141,93.1450949884408,93.2248293335317,93.304521698839,
93.3842009173802,93.4638766811693,93.5435647130373,93.6232807401489,93.7030843030794,
93.7829370277574,93.862903437408,93.9044492067215,93.9844141655087,94.0642847536132,
94.1440784906401,94.2238128357304,94.3035052010373,94.3831844195783,94.4628601833674,
94.5425482152353,94.6222642423477,94.7020678052781,94.7819205299559,94.8618869396063,
94.9034327089207,94.9890127520186,95.0744296002041,95.1596141447421,95.2446560142868,
95.3294979157902,95.3666345040236),.UNSPECIFIED.);
#119=B_SPLINE_CURVE_WITH_KNOTS('',3,(#9934,#9935,#9936,#9937,#9938,#9939,
#9940,#9941,#9942,#9943),.UNSPECIFIED.,.F.,.F.,(4,1,1,1,1,1,1,4),(95.3666347012337,
95.9024162111198,96.901399713319,97.9003832155182,98.8993667177174,99.8983502199165,
100.897333722116,101.649820008413),.UNSPECIFIED.);
#120=B_SPLINE_CURVE_WITH_KNOTS('',3,(#9945,#9946,#9947,#9948,#9949,#9950,
#9951,#9952,#9953,#9954,#9955,#9956,#9957,#9958,#9959,#9960,#9961,#9962,
#9963,#9964,#9965,#9966,#9967,#9968,#9969,#9970,#9971,#9972,#9973,#9974,
#9975,#9976,#9977,#9978,#9979,#9980,#9981,#9982,#9983,#9984,#9985,#9986,
#9987,#9988,#9989,#9990,#9991,#9992,#9993,#9994,#9995,#9996,#9997,#9998,
#9999,#10000,#10001,#10002,#10003,#10004,#10005,#10006,#10007,#10008,#10009,
#10010,#10011,#10012,#10013,#10014,#10015,#10016,#10017,#10018,#10019,#10020,
#10021,#10022,#10023,#10024,#10025,#10026,#10027,#10028,#10029,#10030,#10031,
#10032,#10033,#10034,#10035,#10036,#10037,#10038,#10039,#10040,#10041,#10042,
#10043,#10044,#10045,#10046,#10047,#10048,#10049,#10050,#10051,#10052,#10053,
#10054,#10055,#10056,#10057,#10058,#10059,#10060,#10061,#10062,#10063,#10064,
#10065,#10066,#10067,#10068,#10069,#10070,#10071,#10072,#10073,#10074,#10075,
#10076,#10077,#10078,#10079,#10080,#10081,#10082,#10083,#10084,#10085,#10086,
#10087,#10088,#10089,#10090,#10091,#10092,#10093,#10094,#10095,#10096,#10097,
#10098,#10099,#10100,#10101,#10102,#10103,#10104,#10105,#10106,#10107,#10108,
#10109,#10110,#10111,#10112,#10113,#10114,#10115,#10116,#10117,#10118,#10119,
#10120,#10121,#10122,#10123,#10124,#10125,#10126,#10127,#10128,#10129,#10130,
#10131,#10132,#10133,#10134,#10135,#10136,#10137,#10138,#10139,#10140,#10141,
#10142,#10143,#10144,#10145,#10146,#10147,#10148,#10149,#10150,#10151,#10152,
#10153,#10154,#10155,#10156,#10157,#10158,#10159,#10160,#10161,#10162,#10163,
#10164,#10165,#10166,#10167,#10168,#10169,#10170,#10171,#10172,#10173,#10174,
#10175,#10176,#10177,#10178,#10179,#10180,#10181,#10182,#10183,#10184,#10185,
#10186,#10187,#10188,#10189,#10190,#10191),.UNSPECIFIED.,.F.,.F.,(4,3,3,
3,3,3,3,3,3,3,3,3,3,3,3,3,3,3,3,3,3,3,3,3,3,3,3,3,3,3,3,3,3,3,3,3,3,3,3,
3,3,3,3,3,3,3,3,3,3,3,3,3,3,3,3,3,3,3,3,3,3,3,3,3,3,3,3,3,3,3,3,3,3,3,3,
3,3,3,3,3,3,3,4),(101.649820096463,101.752700226976,101.857939430541,101.896317224315,
101.976282183101,102.056152771205,102.135946508231,102.215680853322,102.295373218628,
102.375052437168,102.454728200956,102.534416232823,102.614132259934,102.693935822864,
102.773788547541,102.85375495719,102.895300726514,102.975265685301,103.055136273406,
103.134930010433,103.214664355524,103.294356720831,103.374035939372,103.453711703162,
103.533399735029,103.613115762141,103.692919325071,103.772772049749,103.8527384594,
103.894284228713,103.9742491875,104.054119775605,104.133913512632,104.213647857723,
104.29334022303,104.373019441571,104.452695205361,104.532383237229,104.61209926434,
104.691902827271,104.771755551949,104.851721961599,104.893267730912,104.973232689699,
105.053103277804,105.132897014831,105.212631359922,105.292323725229,105.37200294377,
105.451678707559,105.531366739427,105.611082766539,105.690886329469,105.770739054147,
105.850705463798,105.892251233112,105.972216191899,106.052086780004,106.131880517031,
106.211614862122,106.291307227429,106.370986445971,106.45066220976,106.530350241628,
106.610066268739,106.68986983167,106.769722556348,106.849688965998,106.891234735311,
106.971199694098,107.051070282203,107.130864019229,107.21059836432,107.290290729627,
107.369969948168,107.449645711957,107.529333743825,107.609049770937,107.688853333867,
107.768706058545,107.848672468195,107.89021823751,107.933005315593),
 .UNSPECIFIED.);
#121=B_SPLINE_CURVE_WITH_KNOTS('',3,(#10193,#10194,#10195,#10196,#10197,
#10198,#10199,#10200,#10201,#10202),.UNSPECIFIED.,.F.,.F.,(4,1,1,1,1,1,
1,4),(107.933011045732,108.889201739709,109.888185241908,110.887168744107,
111.886152246307,112.885135748506,113.884119250705,114.216183287294),
 .UNSPECIFIED.);
#122=B_SPLINE_CURVE_WITH_KNOTS('',3,(#10204,#10205,#10206,#10207,#10208,
#10209,#10210,#10211,#10212,#10213,#10214,#10215,#10216,#10217,#10218,#10219,
#10220,#10221,#10222,#10223,#10224,#10225,#10226,#10227,#10228,#10229,#10230,
#10231,#10232,#10233,#10234,#10235,#10236,#10237,#10238,#10239,#10240,#10241,
#10242,#10243,#10244,#10245,#10246,#10247,#10248,#10249,#10250,#10251,#10252,
#10253,#10254,#10255,#10256,#10257,#10258,#10259,#10260,#10261,#10262,#10263,
#10264,#10265,#10266,#10267,#10268,#10269,#10270,#10271,#10272,#10273,#10274,
#10275,#10276,#10277,#10278,#10279,#10280,#10281,#10282,#10283,#10284,#10285,
#10286,#10287,#10288,#10289,#10290,#10291,#10292,#10293,#10294,#10295,#10296,
#10297,#10298,#10299,#10300,#10301,#10302,#10303,#10304,#10305,#10306,#10307,
#10308,#10309,#10310,#10311,#10312,#10313,#10314,#10315,#10316,#10317,#10318,
#10319,#10320,#10321,#10322,#10323,#10324,#10325,#10326,#10327,#10328,#10329,
#10330,#10331,#10332,#10333,#10334,#10335,#10336,#10337,#10338,#10339,#10340,
#10341,#10342,#10343,#10344,#10345,#10346,#10347,#10348,#10349,#10350,#10351,
#10352,#10353,#10354,#10355,#10356,#10357,#10358,#10359,#10360,#10361,#10362,
#10363,#10364,#10365,#10366,#10367,#10368,#10369,#10370,#10371,#10372,#10373,
#10374,#10375,#10376,#10377,#10378,#10379,#10380,#10381,#10382,#10383,#10384,
#10385,#10386,#10387,#10388,#10389,#10390,#10391,#10392,#10393,#10394,#10395,
#10396,#10397,#10398,#10399,#10400,#10401,#10402,#10403,#10404,#10405,#10406,
#10407,#10408,#10409,#10410,#10411,#10412,#10413,#10414,#10415,#10416,#10417,
#10418,#10419,#10420,#10421,#10422,#10423,#10424,#10425,#10426,#10427,#10428,
#10429,#10430,#10431,#10432,#10433,#10434,#10435,#10436,#10437,#10438,#10439,
#10440,#10441,#10442,#10443,#10444,#10445,#10446,#10447,#10448,#10449,#10450),
 .UNSPECIFIED.,.F.,.F.,(4,3,3,3,3,3,3,3,3,3,3,3,3,3,3,3,3,3,3,3,3,3,3,3,
3,3,3,3,3,3,3,3,3,3,3,3,3,3,3,3,3,3,3,3,3,3,3,3,3,3,3,3,3,3,3,3,3,3,3,3,
3,3,3,3,3,3,3,3,3,3,3,3,3,3,3,3,3,3,3,3,3,3,4),(114.216190622772,114.299554639039,
114.3791579932,114.458764847072,114.538390929541,114.618051978097,114.69780744092,
114.777618197829,114.857543217377,114.883102752904,114.963067711691,115.042938299796,
115.122732036823,115.202466381914,115.28215874722,115.361837965761,115.441513729551,
115.521201761419,115.60091778853,115.68072135146,115.760574076138,115.840540485788,
115.882086255103,115.96205121389,116.041921801995,116.121715539022,116.201449884113,
116.281142249419,116.36082146796,116.44049723175,116.520185263617,116.599901290729,
116.679704853659,116.759557578337,116.839523987988,116.881069757302,116.961034716089,
117.040905304194,117.120699041221,117.200433386311,117.280125751618,117.359804970159,
117.439480733948,117.519168765816,117.598884792928,117.678688355858,117.758541080536,
117.838507490186,117.880053259501,117.960018218289,118.039888806393,118.11968254342,
118.199416888512,118.279109253818,118.35878847236,118.438464236149,118.518152268017,
118.597868295129,118.677671858059,118.757524582737,118.837490992388,118.879036761701,
118.959001720488,119.038872308593,119.11866604562,119.198400390711,119.278092756017,
119.357771974558,119.437447738347,119.517135770216,119.596851797327,119.676655360257,
119.756508084935,119.836474494585,119.8780202639,119.958699782841,120.039280820086,
120.119778432003,120.20020762007,120.280577914094,120.360913170741,120.441236174366,
120.499375929952),.UNSPECIFIED.);
#123=B_SPLINE_CURVE_WITH_KNOTS('',3,(#10452,#10453,#10454,#10455,#10456,
#10457,#10458,#10459,#10460,#10461),.UNSPECIFIED.,.F.,.F.,(4,1,1,1,1,1,
1,4),(120.499383484016,120.877003766099,121.875987268298,122.874970770497,
123.873954272696,124.872937774896,125.871921277095,126.782552527095),
 .UNSPECIFIED.);
#124=B_SPLINE_CURVE_WITH_KNOTS('',3,(#10463,#10464,#10465,#10466,#10467,
#10468,#10469,#10470,#10471,#10472,#10473,#10474,#10475,#10476,#10477,#10478,
#10479,#10480,#10481,#10482,#10483,#10484,#10485,#10486,#10487,#10488,#10489,
#10490,#10491,#10492,#10493,#10494,#10495,#10496,#10497,#10498,#10499,#10500,
#10501,#10502,#10503,#10504,#10505,#10506,#10507,#10508,#10509,#10510,#10511,
#10512,#10513,#10514,#10515,#10516,#10517,#10518,#10519,#10520,#10521,#10522,
#10523,#10524,#10525,#10526,#10527,#10528,#10529,#10530,#10531,#10532,#10533,
#10534,#10535,#10536,#10537,#10538,#10539,#10540,#10541,#10542,#10543,#10544,
#10545,#10546,#10547,#10548,#10549,#10550,#10551,#10552,#10553,#10554,#10555,
#10556,#10557,#10558,#10559,#10560,#10561,#10562,#10563,#10564,#10565,#10566,
#10567,#10568,#10569,#10570,#10571,#10572,#10573,#10574,#10575,#10576,#10577,
#10578,#10579,#10580,#10581,#10582,#10583,#10584,#10585,#10586,#10587,#10588,
#10589,#10590,#10591,#10592,#10593,#10594,#10595,#10596,#10597,#10598,#10599,
#10600,#10601,#10602,#10603,#10604,#10605,#10606,#10607,#10608,#10609,#10610,
#10611,#10612,#10613,#10614,#10615,#10616,#10617,#10618,#10619,#10620,#10621,
#10622,#10623,#10624,#10625,#10626,#10627,#10628,#10629,#10630,#10631,#10632,
#10633,#10634,#10635,#10636,#10637,#10638,#10639,#10640,#10641,#10642,#10643,
#10644,#10645,#10646,#10647,#10648,#10649,#10650,#10651,#10652,#10653,#10654,
#10655,#10656,#10657,#10658,#10659,#10660,#10661,#10662,#10663,#10664,#10665,
#10666,#10667,#10668,#10669,#10670,#10671,#10672,#10673,#10674,#10675,#10676,
#10677,#10678,#10679,#10680,#10681,#10682,#10683,#10684,#10685,#10686,#10687,
#10688,#10689,#10690,#10691,#10692,#10693,#10694,#10695,#10696,#10697,#10698,
#10699,#10700,#10701,#10702,#10703,#10704,#10705,#10706),.UNSPECIFIED.,
 .F.,.F.,(4,3,3,3,3,3,3,3,3,3,3,3,3,3,3,3,3,3,3,3,3,3,3,3,3,3,3,3,3,3,3,
3,3,3,3,3,3,3,3,3,3,3,3,3,3,3,3,3,3,3,3,3,3,3,3,3,3,3,3,3,3,3,3,3,3,3,3,
3,3,3,3,3,3,3,3,3,3,3,3,3,3,4),(126.782561237132,126.870904779294,126.950869738081,
127.030740326186,127.110534063213,127.190268408304,127.269960773611,127.349639992152,
127.429315755941,127.509003787809,127.588719814921,127.668523377851,127.748376102529,
127.82834251218,127.869888281493,127.94985324028,128.029723828385,128.109517565412,
128.189251910503,128.26894427581,128.348623494351,128.42829925814,128.507987290008,
128.587703317119,128.66750688005,128.747359604728,128.827326014378,128.868871783692,
128.948836742479,129.028707330584,129.10850106761,129.188235412701,129.267927778008,
129.347606996549,129.427282760338,129.506970792206,129.586686819317,129.666490382248,
129.746343106926,129.826309516576,129.867855285891,129.947820244679,130.027690832783,
130.10748456981,130.187218914902,130.266911280209,130.34659049875,130.42626626254,
130.505954294408,130.585670321519,130.66547388445,130.745326609128,130.825293018779,
130.866838788091,130.946803746878,131.026674334983,131.10646807201,131.186202417101,
131.265894782408,131.345574000949,131.425249764738,131.504937796606,131.584653823718,
131.664457386648,131.744310111326,131.824276520976,131.86582229029,131.945787249077,
132.025657837182,132.105451574209,132.1851859193,132.264878284606,132.344557503148,
132.424233266937,132.503921298804,132.583637325916,132.663440888846,132.743293613524,
132.823260023174,132.864805792489,132.979172254981,133.065746544311),
 .UNSPECIFIED.);
#125=B_SPLINE_CURVE_WITH_KNOTS('',3,(#10708,#10709,#10710,#10711,#10712,
#10713,#10714,#10715,#10716,#10717,#10718,#10719,#10720,#10721,#10722,#10723,
#10724,#10725,#10726,#10727,#10728,#10729,#10730,#10731,#10732,#10733,#10734,
#10735,#10736,#10737,#10738,#10739,#10740,#10741,#10742,#10743,#10744,#10745,
#10746,#10747,#10748,#10749,#10750,#10751,#10752,#10753,#10754,#10755,#10756,
#10757,#10758,#10759,#10760,#10761,#10762,#10763,#10764,#10765,#10766,#10767,
#10768,#10769,#10770,#10771,#10772,#10773,#10774,#10775,#10776,#10777,#10778,
#10779,#10780,#10781,#10782,#10783,#10784,#10785,#10786,#10787,#10788,#10789,
#10790,#10791,#10792,#10793,#10794,#10795,#10796,#10797,#10798,#10799,#10800,
#10801,#10802,#10803,#10804,#10805,#10806,#10807,#10808,#10809,#10810,#10811,
#10812,#10813,#10814,#10815,#10816,#10817,#10818,#10819,#10820,#10821,#10822,
#10823,#10824,#10825,#10826,#10827,#10828,#10829,#10830,#10831,#10832,#10833,
#10834,#10835,#10836,#10837,#10838,#10839,#10840,#10841,#10842,#10843,#10844,
#10845,#10846,#10847,#10848,#10849,#10850,#10851,#10852,#10853,#10854,#10855,
#10856,#10857,#10858,#10859,#10860,#10861,#10862,#10863,#10864,#10865,#10866,
#10867,#10868,#10869,#10870,#10871,#10872,#10873,#10874,#10875,#10876,#10877,
#10878,#10879,#10880,#10881,#10882,#10883,#10884,#10885,#10886,#10887,#10888,
#10889,#10890,#10891,#10892,#10893,#10894,#10895,#10896,#10897,#10898,#10899,
#10900,#10901,#10902,#10903,#10904,#10905,#10906,#10907,#10908,#10909,#10910,
#10911,#10912,#10913,#10914,#10915,#10916,#10917,#10918,#10919,#10920,#10921,
#10922,#10923,#10924,#10925,#10926,#10927,#10928,#10929,#10930,#10931,#10932,
#10933,#10934,#10935,#10936,#10937,#10938,#10939,#10940,#10941,#10942,#10943,
#10944,#10945,#10946,#10947,#10948,#10949,#10950,#10951),.UNSPECIFIED.,
 .F.,.F.,(4,3,3,3,3,3,3,3,3,3,3,3,3,3,3,3,3,3,3,3,3,3,3,3,3,3,3,3,3,3,3,
3,3,3,3,3,3,3,3,3,3,3,3,3,3,3,3,3,3,3,3,3,3,3,3,3,3,3,3,3,3,3,3,3,3,3,3,
3,3,3,3,3,3,3,3,3,3,3,3,3,3,4),(133.065746544471,133.144414831246,133.223020181614,
133.303116320748,133.381660781291,133.460201368281,133.538754623018,133.620013290935,
133.698682056643,133.781235675665,133.863789294688,133.943754253475,134.02362484158,
134.103418578607,134.183152923698,134.262845289004,134.342524507545,134.422200271334,
134.501888303202,134.581604330314,134.661407893244,134.741260617922,134.821227027572,
134.862772796887,134.942737755674,135.022608343779,135.102402080806,135.182136425896,
135.261828791203,135.341508009744,135.421183773533,135.500871805401,135.580587832512,
135.660391395442,135.74024412012,135.820210529771,135.861756299086,135.941721257874,
136.021591845978,136.101385583006,136.181119928097,136.260812293404,136.340491511945,
136.420167275735,136.499855307603,136.579571334715,136.659374897646,136.739227622324,
136.819194031975,136.860739801286,136.940704760073,137.020575348178,137.100369085205,
137.180103430296,137.259795795603,137.339475014144,137.419150777933,137.498838809801,
137.578554836913,137.658358399843,137.738211124521,137.818177534172,137.859723303485,
137.939688262272,138.019558850377,138.099352587403,138.179086932494,138.258779297802,
138.338458516343,138.418134280132,138.497822311999,138.577538339111,138.657341902041,
138.737194626718,138.817161036368,138.858706805684,138.943144794911,139.027438869103,
139.111535628609,139.195515746164,139.279334149676,139.34893185139),
 .UNSPECIFIED.);
#126=B_SPLINE_CURVE_WITH_KNOTS('',3,(#10953,#10954,#10955,#10956,#10957,
#10958,#10959,#10960,#10961,#10962,#10963,#10964,#10965,#10966,#10967,#10968,
#10969,#10970,#10971,#10972,#10973,#10974,#10975,#10976,#10977,#10978,#10979,
#10980,#10981,#10982,#10983,#10984,#10985,#10986,#10987,#10988,#10989,#10990,
#10991,#10992,#10993,#10994,#10995,#10996,#10997,#10998,#10999,#11000,#11001,
#11002,#11003,#11004,#11005,#11006,#11007,#11008,#11009,#11010,#11011,#11012,
#11013,#11014,#11015,#11016,#11017,#11018,#11019,#11020,#11021,#11022,#11023,
#11024,#11025,#11026,#11027,#11028,#11029,#11030,#11031,#11032,#11033,#11034,
#11035,#11036,#11037,#11038,#11039,#11040,#11041,#11042,#11043,#11044,#11045,
#11046,#11047,#11048,#11049,#11050,#11051,#11052,#11053,#11054,#11055,#11056,
#11057,#11058,#11059,#11060,#11061,#11062,#11063,#11064,#11065,#11066,#11067,
#11068,#11069,#11070,#11071,#11072,#11073,#11074,#11075,#11076,#11077,#11078,
#11079,#11080,#11081,#11082,#11083,#11084,#11085,#11086,#11087,#11088,#11089,
#11090,#11091,#11092,#11093,#11094,#11095,#11096,#11097,#11098,#11099,#11100,
#11101,#11102,#11103,#11104,#11105,#11106,#11107,#11108,#11109,#11110,#11111,
#11112,#11113,#11114,#11115,#11116,#11117,#11118,#11119,#11120,#11121,#11122,
#11123,#11124,#11125,#11126,#11127,#11128,#11129,#11130,#11131,#11132,#11133,
#11134,#11135,#11136,#11137,#11138,#11139,#11140,#11141,#11142,#11143,#11144,
#11145,#11146,#11147,#11148,#11149,#11150,#11151,#11152,#11153,#11154,#11155,
#11156,#11157,#11158,#11159,#11160,#11161,#11162,#11163,#11164,#11165,#11166,
#11167,#11168,#11169,#11170,#11171,#11172,#11173,#11174,#11175,#11176,#11177,
#11178,#11179,#11180,#11181,#11182,#11183,#11184,#11185,#11186,#11187,#11188,
#11189,#11190,#11191,#11192,#11193,#11194,#11195,#11196),.UNSPECIFIED.,
 .F.,.F.,(4,3,3,3,3,3,3,3,3,3,3,3,3,3,3,3,3,3,3,3,3,3,3,3,3,3,3,3,3,3,3,
3,3,3,3,3,3,3,3,3,3,3,3,3,3,3,3,3,3,3,3,3,3,3,3,3,3,3,3,3,3,3,3,3,3,3,3,
3,3,3,3,3,3,3,3,3,3,3,3,3,3,4),(139.348931851491,139.432079150989,139.515320103915,
139.600912654907,139.684429370585,139.771059839234,139.857690307883,139.93765526667,
140.017525854775,140.097319591802,140.177053936893,140.256746302201,140.336425520742,
140.416101284531,140.495789316399,140.575505343511,140.655308906441,140.735161631119,
140.81512804077,140.856673810082,140.936638768869,141.016509356974,141.096303094,
141.176037439091,141.255729804398,141.335409022939,141.415084786728,141.494772818596,
141.574488845707,141.654292408638,141.734145133316,141.814111542966,141.855657312281,
141.935622271068,142.015492859173,142.0952865962,142.175020941292,142.254713306599,
142.33439252514,142.41406828893,142.493756320798,142.573472347909,142.65327591084,
142.733128635518,142.813095045169,142.854640814481,142.934605773268,143.014476361373,
143.0942700984,143.174004443491,143.253696808799,143.33337602734,143.413051791129,
143.492739822997,143.572455850108,143.652259413038,143.732112137716,143.812078547367,
143.85362431668,143.933589275467,144.013459863571,144.093253600598,144.172987945689,
144.252680310997,144.332359529538,144.412035293327,144.491723325195,144.571439352307,
144.651242915237,144.731095639916,144.811062049566,144.852607818879,144.931490161362,
145.010277469427,145.08897511628,145.167622082638,145.24623491863,145.324830146253,
145.403451165995,145.482083209498,145.560786285368,145.63211715867),
 .UNSPECIFIED.);
#127=B_SPLINE_CURVE_WITH_KNOTS('',3,(#11198,#11199,#11200,#11201,#11202,
#11203,#11204,#11205,#11206,#11207,#11208),.UNSPECIFIED.,.F.,.F.,(4,1,1,
1,1,1,1,1,4),(145.63211715867,145.851591321078,146.850574823277,147.849558325476,
148.848541827676,149.847525329875,150.846508832074,151.845492334273,151.91530246585),
 .UNSPECIFIED.);
#128=B_SPLINE_CURVE_WITH_KNOTS('',3,(#11210,#11211,#11212,#11213,#11214,
#11215,#11216,#11217,#11218,#11219,#11220,#11221,#11222,#11223,#11224,#11225,
#11226,#11227,#11228,#11229,#11230,#11231,#11232,#11233,#11234,#11235,#11236,
#11237,#11238,#11239,#11240,#11241,#11242,#11243,#11244,#11245,#11246,#11247,
#11248,#11249,#11250,#11251,#11252,#11253,#11254,#11255,#11256,#11257,#11258,
#11259,#11260,#11261,#11262,#11263,#11264,#11265,#11266,#11267,#11268,#11269,
#11270,#11271,#11272,#11273,#11274,#11275,#11276,#11277,#11278,#11279,#11280,
#11281,#11282,#11283,#11284,#11285,#11286,#11287,#11288,#11289,#11290,#11291,
#11292,#11293,#11294,#11295,#11296,#11297,#11298,#11299,#11300,#11301,#11302,
#11303,#11304,#11305,#11306,#11307,#11308,#11309,#11310,#11311,#11312,#11313,
#11314,#11315,#11316,#11317,#11318,#11319,#11320,#11321,#11322,#11323,#11324,
#11325,#11326,#11327,#11328,#11329,#11330,#11331,#11332,#11333,#11334,#11335,
#11336,#11337,#11338,#11339,#11340,#11341,#11342,#11343,#11344,#11345,#11346,
#11347,#11348,#11349,#11350,#11351,#11352,#11353,#11354,#11355,#11356,#11357,
#11358,#11359,#11360,#11361,#11362,#11363,#11364,#11365,#11366,#11367,#11368,
#11369,#11370,#11371,#11372,#11373,#11374,#11375,#11376,#11377,#11378,#11379,
#11380,#11381,#11382,#11383,#11384,#11385,#11386,#11387,#11388,#11389,#11390,
#11391,#11392,#11393,#11394,#11395,#11396,#11397,#11398,#11399,#11400,#11401,
#11402,#11403,#11404,#11405,#11406,#11407,#11408,#11409,#11410,#11411,#11412,
#11413,#11414,#11415,#11416,#11417,#11418,#11419,#11420,#11421,#11422,#11423,
#11424,#11425,#11426,#11427,#11428,#11429,#11430,#11431,#11432,#11433,#11434,
#11435,#11436,#11437,#11438,#11439,#11440,#11441,#11442,#11443,#11444,#11445,
#11446,#11447,#11448,#11449,#11450,#11451,#11452,#11453),.UNSPECIFIED.,
 .F.,.F.,(4,3,3,3,3,3,3,3,3,3,3,3,3,3,3,3,3,3,3,3,3,3,3,3,3,3,3,3,3,3,3,
3,3,3,3,3,3,3,3,3,3,3,3,3,3,3,3,3,3,3,3,3,3,3,3,3,3,3,3,3,3,3,3,3,3,3,3,
3,3,3,3,3,3,3,3,3,3,3,3,3,3,4),(151.91530246585,151.994451245667,152.073510801261,
152.152499317386,152.231434913233,152.310343716248,152.389240399023,152.468141288704,
152.547062713042,152.626066282013,152.705113451247,152.784277825896,152.844475836472,
152.924440795259,153.004311383364,153.08410512039,153.163839465482,153.243531830788,
153.323211049329,153.402886813118,153.482574844986,153.562290872097,153.642094435027,
153.721947159705,153.801913569355,153.843459338671,153.923424297459,154.003294885564,
154.083088622591,154.162822967682,154.242515332989,154.32219455153,154.401870315319,
154.481558347188,154.5612743743,154.641077937231,154.720930661909,154.800897071559,
154.842442840871,154.922407799658,155.002278387763,155.08207212479,155.161806469881,
155.241498835188,155.321178053729,155.400853817518,155.480541849386,155.560257876498,
155.640061439428,155.719914164106,155.799880573757,155.84142634307,155.921391301857,
156.001261889962,156.081055626988,156.160789972079,156.240482337386,156.320161555927,
156.399837319716,156.479525351584,156.559241378695,156.639044941626,156.718897666304,
156.798864075954,156.840409845269,156.920374804056,157.000245392161,157.080039129188,
157.159773474279,157.239465839586,157.319145058127,157.398820821916,157.478508853784,
157.558224880895,157.638028443826,157.717881168503,157.797847578154,157.839393347468,
157.931101851476,158.022495910503,158.113268253516,158.198487526203),
 .UNSPECIFIED.);
#129=B_SPLINE_CURVE_WITH_KNOTS('',3,(#11455,#11456,#11457,#11458,#11459,
#11460,#11461,#11462,#11463,#11464),.UNSPECIFIED.,.F.,.F.,(4,1,1,1,1,1,
1,4),(158.198487773029,158.838376849667,159.837360351866,160.836343854066,
161.835327356265,162.834310858464,163.833294360663,164.481673080209),
 .UNSPECIFIED.);
#130=B_SPLINE_CURVE_WITH_KNOTS('',3,(#11466,#11467,#11468,#11469,#11470,
#11471,#11472,#11473,#11474,#11475,#11476,#11477,#11478,#11479,#11480,#11481,
#11482,#11483,#11484,#11485,#11486,#11487,#11488,#11489,#11490,#11491,#11492,
#11493,#11494,#11495,#11496,#11497,#11498,#11499,#11500,#11501,#11502,#11503,
#11504,#11505,#11506,#11507,#11508,#11509,#11510,#11511,#11512,#11513,#11514,
#11515,#11516,#11517,#11518,#11519,#11520,#11521,#11522,#11523,#11524,#11525,
#11526,#11527,#11528,#11529,#11530,#11531,#11532,#11533,#11534,#11535,#11536,
#11537,#11538,#11539,#11540,#11541,#11542,#11543,#11544,#11545,#11546,#11547,
#11548,#11549,#11550,#11551,#11552,#11553,#11554,#11555,#11556,#11557,#11558,
#11559,#11560,#11561,#11562,#11563,#11564,#11565,#11566,#11567,#11568,#11569,
#11570,#11571,#11572,#11573,#11574,#11575,#11576,#11577,#11578,#11579,#11580,
#11581,#11582,#11583,#11584,#11585,#11586,#11587,#11588,#11589,#11590,#11591,
#11592,#11593,#11594,#11595,#11596,#11597,#11598,#11599,#11600,#11601,#11602,
#11603,#11604,#11605,#11606,#11607,#11608,#11609,#11610,#11611,#11612,#11613,
#11614,#11615,#11616,#11617,#11618,#11619,#11620,#11621,#11622,#11623,#11624,
#11625,#11626,#11627,#11628,#11629,#11630,#11631,#11632,#11633,#11634,#11635,
#11636,#11637,#11638,#11639,#11640,#11641,#11642,#11643,#11644,#11645,#11646,
#11647,#11648,#11649,#11650,#11651,#11652,#11653,#11654,#11655,#11656,#11657,
#11658,#11659,#11660,#11661,#11662,#11663,#11664,#11665,#11666,#11667,#11668,
#11669,#11670,#11671,#11672,#11673,#11674,#11675,#11676,#11677,#11678,#11679,
#11680,#11681,#11682,#11683,#11684,#11685,#11686,#11687,#11688,#11689,#11690,
#11691,#11692,#11693,#11694,#11695,#11696,#11697,#11698,#11699,#11700,#11701,
#11702,#11703,#11704,#11705,#11706,#11707,#11708,#11709),.UNSPECIFIED.,
 .F.,.F.,(4,3,3,3,3,3,3,3,3,3,3,3,3,3,3,3,3,3,3,3,3,3,3,3,3,3,3,3,3,3,3,
3,3,3,3,3,3,3,3,3,3,3,3,3,3,3,3,3,3,3,3,3,3,3,3,3,3,3,3,3,3,3,3,3,3,3,3,
3,3,3,3,3,3,3,3,3,3,3,3,3,3,4),(164.481673325019,164.573090933397,164.66493832906,
164.757357139414,164.832277862862,164.91224282165,164.992113409754,165.071907146782,
165.151641491873,165.23133385718,165.311013075721,165.390688839511,165.470376871379,
165.550092898491,165.629896461422,165.7097491861,165.789715595751,165.831261365061,
165.911226323848,165.991096911953,166.07089064898,166.150624994072,166.230317359378,
166.30999657792,166.389672341709,166.469360373577,166.549076400689,166.628879963619,
166.708732688298,166.788699097948,166.830244867261,166.910209826048,166.990080414153,
167.06987415118,167.149608496271,167.229300861577,167.308980080119,167.388655843908,
167.468343875776,167.548059902887,167.627863465818,167.707716190495,167.787682600146,
167.82922836946,167.909193328247,167.989063916352,168.068857653378,168.148591998469,
168.228284363776,168.307963582317,168.387639346106,168.467327377974,168.547043405086,
168.626846968016,168.706699692694,168.786666102344,168.828211871659,168.908176830446,
168.988047418551,169.067841155578,169.147575500669,169.227267865975,169.306947084517,
169.386622848306,169.466310880174,169.546026907285,169.625830470216,169.705683194894,
169.785649604544,169.827195373858,169.906442099061,169.985594953595,170.064672086523,
170.143691578133,170.222677307682,170.301646466472,170.380615335551,170.45960019336,
170.53866168693,170.617762731622,170.696978651885,170.764858387389),
 .UNSPECIFIED.);
#131=B_SPLINE_CURVE_WITH_KNOTS('',3,(#11711,#11712,#11713,#11714,#11715,
#11716,#11717,#11718,#11719,#11720,#11721,#11722),.UNSPECIFIED.,.F.,.F.,
(4,2,1,1,1,1,1,1,4),(170.764858387389,170.826178876057,171.825162378256,
172.824145880456,173.823129382655,174.822112884854,175.821096387053,176.820079889252,
177.048043694568),.UNSPECIFIED.);
#132=B_SPLINE_CURVE_WITH_KNOTS('',3,(#11724,#11725,#11726,#11727,#11728,
#11729,#11730,#11731,#11732,#11733),.UNSPECIFIED.,.F.,.F.,(4,1,1,1,1,1,
1,4),(177.048043694568,177.819063391451,178.818046893651,179.81703039585,
180.816013898049,181.814997400248,182.813980902447,183.331229001748),
 .UNSPECIFIED.);
#133=B_SPLINE_CURVE_WITH_KNOTS('',3,(#11735,#11736,#11737,#11738,#11739,
#11740,#11741,#11742,#11743,#11744),.UNSPECIFIED.,.F.,.F.,(4,1,1,1,1,1,
1,4),(183.331229001748,183.812964404646,184.811947906846,185.810931409045,
186.809914911244,187.808898413443,188.807881915642,189.614410347781),
 .UNSPECIFIED.);
#134=B_SPLINE_CURVE_WITH_KNOTS('',3,(#11746,#11747,#11748,#11749,#11750,
#11751,#11752,#11753,#11754,#11755,#11756,#11757,#11758,#11759,#11760,#11761,
#11762,#11763,#11764,#11765,#11766,#11767,#11768,#11769,#11770,#11771,#11772,
#11773,#11774,#11775,#11776,#11777,#11778,#11779,#11780,#11781,#11782,#11783,
#11784,#11785,#11786,#11787,#11788,#11789,#11790,#11791,#11792,#11793,#11794,
#11795,#11796,#11797,#11798,#11799,#11800,#11801,#11802,#11803,#11804,#11805,
#11806,#11807,#11808,#11809,#11810,#11811,#11812,#11813,#11814,#11815,#11816,
#11817,#11818,#11819,#11820,#11821,#11822,#11823,#11824,#11825,#11826,#11827,
#11828,#11829,#11830,#11831,#11832,#11833,#11834,#11835,#11836,#11837,#11838,
#11839,#11840,#11841,#11842,#11843,#11844,#11845,#11846,#11847,#11848,#11849,
#11850,#11851,#11852,#11853,#11854,#11855,#11856,#11857,#11858,#11859,#11860,
#11861,#11862,#11863,#11864,#11865,#11866,#11867,#11868,#11869,#11870,#11871,
#11872,#11873,#11874,#11875,#11876,#11877,#11878,#11879,#11880,#11881,#11882,
#11883,#11884,#11885,#11886,#11887,#11888,#11889,#11890,#11891,#11892,#11893,
#11894,#11895,#11896,#11897,#11898,#11899,#11900,#11901,#11902,#11903,#11904,
#11905,#11906,#11907,#11908,#11909,#11910,#11911,#11912,#11913,#11914,#11915,
#11916,#11917,#11918,#11919,#11920,#11921,#11922,#11923,#11924,#11925,#11926,
#11927,#11928,#11929,#11930,#11931,#11932,#11933,#11934,#11935,#11936,#11937,
#11938,#11939,#11940,#11941,#11942,#11943,#11944,#11945,#11946,#11947,#11948,
#11949,#11950,#11951,#11952,#11953,#11954,#11955,#11956,#11957,#11958,#11959,
#11960,#11961,#11962,#11963,#11964,#11965,#11966,#11967,#11968,#11969,#11970,
#11971,#11972,#11973,#11974,#11975,#11976,#11977,#11978,#11979,#11980,#11981,
#11982,#11983,#11984,#11985,#11986,#11987,#11988,#11989),.UNSPECIFIED.,
 .F.,.F.,(4,3,3,3,3,3,3,3,3,3,3,3,3,3,3,3,3,3,3,3,3,3,3,3,3,3,3,3,3,3,3,
3,3,3,3,3,3,3,3,3,3,3,3,3,3,3,3,3,3,3,3,3,3,3,3,3,3,3,3,3,3,3,3,3,3,3,3,
3,3,3,3,3,3,3,3,3,3,3,3,3,3,4),(189.614414308927,189.731351580901,189.806865417841,
189.886830376629,189.966700964734,190.046494701761,190.126229046853,190.20592141216,
190.285600630701,190.365276394491,190.444964426359,190.524680453471,190.604484016402,
190.68433674108,190.764303150731,190.805848920041,190.885813878828,190.965684466933,
191.04547820396,191.125212549051,191.204904914357,191.284584132899,191.364259896688,
191.443947928555,191.523663955667,191.603467518597,191.683320243275,191.763286652926,
191.80483242224,191.884797381027,191.964667969132,192.044461706159,192.12419605125,
192.203888416556,192.283567635098,192.363243398887,192.442931430754,192.522647457866,
192.602451020796,192.682303745474,192.762270155124,192.803815924439,192.883780883226,
192.963651471331,193.043445208358,193.123179553449,193.202871918756,193.282551137297,
193.362226901086,193.441914932954,193.521630960065,193.601434522996,193.681287247674,
193.761253657324,193.802799426638,193.882764385425,193.96263497353,194.042428710557,
194.122163055648,194.201855420955,194.281534639496,194.361210403285,194.440898435153,
194.520614462264,194.600418025195,194.680270749873,194.760237159523,194.801782928837,
194.881747887624,194.961618475729,195.041412212755,195.121146557846,195.200838923153,
195.280518141694,195.360193905483,195.439881937351,195.519597964462,195.599401527393,
195.679254252071,195.759220661721,195.800766431036,195.897599616107),
 .UNSPECIFIED.);
#135=B_SPLINE_CURVE_WITH_KNOTS('',3,(#11991,#11992,#11993,#11994,#11995,
#11996,#11997,#11998,#11999,#12000),.UNSPECIFIED.,.F.,.F.,(4,1,1,1,1,1,
1,4),(195.897608625592,196.799749933236,197.798733435435,198.797716937634,
199.796700439833,200.795683942032,201.794667444231,202.180777541694),
 .UNSPECIFIED.);
#136=B_SPLINE_CURVE_WITH_KNOTS('',3,(#12002,#12003,#12004,#12005,#12006,
#12007,#12008,#12009,#12010,#12011,#12012,#12013,#12014,#12015,#12016,#12017,
#12018,#12019,#12020,#12021,#12022,#12023,#12024,#12025,#12026,#12027,#12028,
#12029,#12030,#12031,#12032,#12033,#12034,#12035,#12036,#12037,#12038,#12039,
#12040,#12041,#12042,#12043,#12044,#12045,#12046,#12047,#12048,#12049,#12050,
#12051,#12052,#12053,#12054,#12055,#12056,#12057,#12058,#12059,#12060,#12061,
#12062,#12063,#12064,#12065,#12066,#12067,#12068,#12069,#12070,#12071,#12072,
#12073,#12074,#12075,#12076,#12077,#12078,#12079,#12080,#12081,#12082,#12083,
#12084,#12085,#12086,#12087,#12088,#12089,#12090,#12091,#12092,#12093,#12094,
#12095,#12096,#12097,#12098,#12099,#12100,#12101,#12102,#12103,#12104,#12105,
#12106,#12107,#12108,#12109,#12110,#12111,#12112,#12113,#12114,#12115,#12116,
#12117,#12118,#12119,#12120,#12121,#12122,#12123,#12124,#12125,#12126,#12127,
#12128,#12129,#12130,#12131,#12132,#12133,#12134,#12135,#12136,#12137,#12138,
#12139,#12140,#12141,#12142,#12143,#12144,#12145,#12146,#12147,#12148,#12149,
#12150,#12151,#12152,#12153,#12154,#12155,#12156,#12157,#12158,#12159,#12160,
#12161,#12162,#12163,#12164,#12165,#12166,#12167,#12168,#12169,#12170,#12171,
#12172,#12173,#12174,#12175,#12176,#12177,#12178,#12179,#12180,#12181,#12182,
#12183,#12184,#12185,#12186,#12187,#12188,#12189,#12190,#12191,#12192,#12193,
#12194,#12195,#12196,#12197,#12198,#12199,#12200,#12201,#12202,#12203,#12204,
#12205,#12206,#12207,#12208,#12209,#12210,#12211,#12212,#12213,#12214,#12215,
#12216,#12217,#12218,#12219,#12220,#12221,#12222,#12223,#12224,#12225,#12226,
#12227,#12228,#12229,#12230,#12231,#12232,#12233,#12234,#12235,#12236,#12237,
#12238,#12239,#12240,#12241,#12242,#12243,#12244,#12245,#12246,#12247,#12248),
 .UNSPECIFIED.,.F.,.F.,(4,3,3,3,3,3,3,3,3,3,3,3,3,3,3,3,3,3,3,3,3,3,3,3,
3,3,3,3,3,3,3,3,3,3,3,3,3,3,3,3,3,3,3,3,3,3,3,3,3,3,3,3,3,3,3,3,3,3,3,3,
3,3,3,3,3,3,3,3,3,3,3,3,3,3,3,3,3,3,3,3,3,3,4),(202.180784923286,202.261270285153,
202.341767965932,202.422292615556,202.502858897515,202.583532018821,202.664264123885,
202.745126086351,202.793650946431,202.873615905218,202.953486493322,203.033280230349,
203.11301457544,203.192706940747,203.272386159288,203.352061923077,203.431749954945,
203.511465982056,203.591269544986,203.671122269664,203.751088679314,203.79263444863,
203.872599407417,203.952469995522,204.032263732548,204.111998077639,204.191690442946,
204.271369661487,204.351045425276,204.430733457144,204.510449484255,204.590253047186,
204.670105771864,204.750072181514,204.791617950829,204.871582909616,204.951453497721,
205.031247234748,205.110981579839,205.190673945146,205.270353163687,205.350028927476,
205.429716959344,205.509432986456,205.589236549387,205.669089274065,205.749055683715,
205.790601453028,205.870566411815,205.95043699992,206.030230736947,206.109965082037,
206.189657447344,206.269336665885,206.349012429674,206.428700461542,206.508416488653,
206.588220051583,206.668072776261,206.748039185911,206.789584955227,206.869549914014,
206.949420502119,207.029214239145,207.108948584236,207.188640949543,207.268320168084,
207.347995931873,207.427683963741,207.507399990853,207.587203553783,207.667056278461,
207.747022688111,207.788568457426,207.8683838667,207.948070824655,208.027682813139,
208.107235768938,208.186745588199,208.266236013343,208.345714799917,208.425214991925,
208.463970230466),.UNSPECIFIED.);
#137=B_SPLINE_CURVE_WITH_KNOTS('',3,(#12250,#12251,#12252,#12253,#12254,
#12255,#12256,#12257,#12258,#12259),.UNSPECIFIED.,.F.,.F.,(4,1,1,1,1,1,
1,4),(208.463977261698,208.787551959626,209.786535461825,210.785518964024,
211.784502466223,212.783485968422,213.782469470621,214.747150895081),
 .UNSPECIFIED.);
#138=B_SPLINE_CURVE_WITH_KNOTS('',3,(#12261,#12262,#12263,#12264,#12265,
#12266,#12267,#12268,#12269,#12270,#12271,#12272,#12273,#12274,#12275,#12276,
#12277,#12278,#12279,#12280,#12281,#12282,#12283,#12284,#12285,#12286,#12287,
#12288,#12289,#12290,#12291,#12292,#12293,#12294,#12295,#12296,#12297,#12298,
#12299,#12300,#12301,#12302,#12303,#12304,#12305,#12306,#12307,#12308,#12309,
#12310,#12311,#12312,#12313,#12314,#12315,#12316,#12317,#12318,#12319,#12320,
#12321,#12322,#12323,#12324,#12325,#12326,#12327,#12328,#12329,#12330,#12331,
#12332,#12333,#12334,#12335,#12336,#12337,#12338,#12339,#12340,#12341,#12342,
#12343,#12344,#12345,#12346,#12347,#12348,#12349,#12350,#12351,#12352,#12353,
#12354,#12355,#12356,#12357,#12358,#12359,#12360,#12361,#12362,#12363,#12364,
#12365,#12366,#12367,#12368,#12369,#12370,#12371,#12372,#12373,#12374,#12375,
#12376,#12377,#12378,#12379,#12380,#12381,#12382,#12383,#12384,#12385,#12386,
#12387,#12388,#12389,#12390,#12391,#12392,#12393,#12394,#12395,#12396,#12397,
#12398,#12399,#12400,#12401,#12402,#12403,#12404,#12405,#12406,#12407,#12408,
#12409,#12410,#12411,#12412,#12413,#12414,#12415,#12416,#12417,#12418,#12419,
#12420,#12421,#12422,#12423,#12424,#12425,#12426,#12427,#12428,#12429,#12430,
#12431,#12432,#12433,#12434,#12435,#12436,#12437,#12438,#12439,#12440,#12441,
#12442,#12443,#12444,#12445,#12446,#12447,#12448,#12449,#12450,#12451,#12452,
#12453,#12454,#12455,#12456,#12457,#12458,#12459,#12460,#12461,#12462,#12463,
#12464,#12465,#12466,#12467,#12468,#12469,#12470,#12471,#12472,#12473,#12474,
#12475,#12476,#12477,#12478,#12479,#12480,#12481,#12482,#12483,#12484,#12485,
#12486,#12487,#12488,#12489,#12490,#12491,#12492,#12493,#12494,#12495,#12496,
#12497,#12498,#12499,#12500,#12501,#12502,#12503,#12504,#12505,#12506,#12507),
 .UNSPECIFIED.,.F.,.F.,(4,3,3,3,3,3,3,3,3,3,3,3,3,3,3,3,3,3,3,3,3,3,3,3,
3,3,3,3,3,3,3,3,3,3,3,3,3,3,3,3,3,3,3,3,3,3,3,3,3,3,3,3,3,3,3,3,3,3,3,3,
3,3,3,3,3,3,3,3,3,3,3,3,3,3,3,3,3,3,3,3,3,3,4),(214.747155537646,214.781452972821,
214.861417931608,214.941288519713,215.02108225674,215.100816601831,215.180508967138,
215.260188185679,215.339863949469,215.419551981337,215.499268008448,215.579071571379,
215.658924296057,215.738890705707,215.78043647502,215.860401433807,215.940272021912,
216.020065758939,216.09980010403,216.179492469337,216.259171687878,216.338847451667,
216.418535483535,216.498251510646,216.578055073577,216.657907798255,216.737874207905,
216.779419977219,216.859384936006,216.939255524111,217.019049261138,217.098783606229,
217.178475971535,217.258155190077,217.337830953866,217.417518985733,217.497235012845,
217.577038575775,217.656891300453,217.736857710104,217.778403479418,217.858368438205,
217.93823902631,218.018032763337,218.097767108428,218.177459473735,218.257138692276,
218.336814456065,218.416502487933,218.496218515044,218.576022077975,218.655874802653,
218.735841212303,218.777386981617,218.857351940404,218.937222528509,219.017016265535,
219.096750610627,219.176442975933,219.256122194474,219.335797958263,219.415485990131,
219.495202017243,219.575005580173,219.654858304851,219.734824714501,219.776370483816,
219.856335442603,219.936206030708,220.015999767735,220.095734112826,220.175426478133,
220.255105696675,220.334781460464,220.414469492332,220.494185519444,220.573989082374,
220.653841807052,220.733808216703,220.775353986016,220.87922915492,220.981055161892,
221.03034077524),.UNSPECIFIED.);
#139=B_SPLINE_CURVE_WITH_KNOTS('',3,(#12509,#12510,#12511,#12512,#12513,
#12514,#12515,#12516,#12517,#12518),.UNSPECIFIED.,.F.,.F.,(4,1,1,1,1,1,
1,4),(221.030340844825,221.774337488215,222.773320990414,223.772304492613,
224.771287994812,225.770271497011,226.76925499921,227.313526152005),
 .UNSPECIFIED.);
#140=B_SPLINE_CURVE_WITH_KNOTS('',3,(#12520,#12521,#12522,#12523,#12524,
#12525,#12526,#12527,#12528,#12529),.UNSPECIFIED.,.F.,.F.,(4,1,1,1,1,1,
1,4),(227.313526152005,227.76823850141,228.767222003609,229.766205505808,
230.765189008007,231.764172510206,232.763156012406,233.596711459184),
 .UNSPECIFIED.);
#141=B_SPLINE_CURVE_WITH_KNOTS('',3,(#12531,#12532,#12533,#12534,#12535,
#12536,#12537,#12538,#12539,#12540,#12541),.UNSPECIFIED.,.F.,.F.,(4,1,1,
1,1,1,1,1,4),(233.596711459184,233.762139514605,234.761123016804,235.760106519003,
236.759090021202,237.758073523401,238.7570570256,239.7560405278,239.879896766364),
 .UNSPECIFIED.);
#142=B_SPLINE_CURVE_WITH_KNOTS('',3,(#12543,#12544,#12545,#12546,#12547,
#12548,#12549,#12550,#12551,#12552,#12553,#12554,#12555,#12556,#12557,#12558,
#12559,#12560,#12561,#12562,#12563,#12564,#12565,#12566,#12567,#12568,#12569,
#12570,#12571,#12572,#12573,#12574,#12575,#12576,#12577,#12578,#12579,#12580,
#12581,#12582,#12583,#12584,#12585,#12586,#12587,#12588,#12589,#12590,#12591,
#12592,#12593,#12594,#12595,#12596,#12597,#12598,#12599,#12600,#12601,#12602,
#12603,#12604,#12605,#12606,#12607,#12608,#12609,#12610,#12611,#12612,#12613,
#12614,#12615,#12616,#12617,#12618,#12619,#12620,#12621,#12622,#12623,#12624,
#12625,#12626,#12627,#12628,#12629,#12630,#12631,#12632,#12633,#12634,#12635,
#12636,#12637,#12638,#12639,#12640,#12641,#12642,#12643,#12644,#12645,#12646,
#12647,#12648,#12649,#12650,#12651,#12652,#12653,#12654,#12655,#12656,#12657,
#12658,#12659,#12660,#12661,#12662,#12663,#12664,#12665,#12666,#12667,#12668,
#12669,#12670,#12671,#12672,#12673,#12674,#12675,#12676,#12677,#12678,#12679,
#12680,#12681,#12682,#12683,#12684,#12685,#12686,#12687,#12688,#12689,#12690,
#12691,#12692,#12693,#12694,#12695,#12696,#12697,#12698,#12699,#12700,#12701,
#12702,#12703,#12704,#12705,#12706,#12707,#12708,#12709,#12710,#12711,#12712,
#12713,#12714,#12715,#12716,#12717,#12718,#12719,#12720,#12721,#12722,#12723,
#12724,#12725,#12726,#12727,#12728,#12729,#12730,#12731,#12732,#12733,#12734,
#12735,#12736,#12737,#12738,#12739,#12740,#12741,#12742,#12743,#12744,#12745,
#12746,#12747,#12748,#12749,#12750,#12751,#12752,#12753,#12754,#12755,#12756,
#12757,#12758,#12759,#12760,#12761,#12762,#12763,#12764,#12765,#12766,#12767,
#12768,#12769,#12770,#12771,#12772,#12773,#12774,#12775,#12776,#12777,#12778,
#12779,#12780,#12781,#12782,#12783,#12784,#12785,#12786),.UNSPECIFIED.,
 .F.,.F.,(4,3,3,3,3,3,3,3,3,3,3,3,3,3,3,3,3,3,3,3,3,3,3,3,3,3,3,3,3,3,3,
3,3,3,3,3,3,3,3,3,3,3,3,3,3,3,3,3,3,3,3,3,3,3,3,3,3,3,3,3,3,3,3,3,3,3,3,
3,3,3,3,3,3,3,3,3,3,3,3,3,3,4),(239.879896766364,239.958682331775,240.03738738754,
240.116030307585,240.195904522887,240.274488338953,240.353068882816,240.431662673636,
240.512503012727,240.591212968301,240.67311849915,240.755024029999,240.834988988786,
240.914859576891,240.994653313918,241.074387659009,241.154080024316,241.233759242857,
241.313435006646,241.393123038514,241.472839065625,241.552642628555,241.632495353233,
241.712461762884,241.754007532198,241.833972490985,241.91384307909,241.993636816117,
242.073371161208,242.153063526515,242.232742745056,242.312418508845,242.392106540713,
242.471822567825,242.551626130756,242.631478855433,242.711445265084,242.752991034397,
242.832955993184,242.912826581289,242.992620318316,243.072354663407,243.152047028714,
243.231726247255,243.311402011045,243.391090042912,243.470806070024,243.550609632955,
243.630462357633,243.710428767283,243.751974536596,243.831939495383,243.911810083488,
243.991603820514,244.071338165605,244.151030530912,244.230709749453,244.310385513242,
244.39007354511,244.469789572222,244.549593135152,244.629445859829,244.70941226948,
244.750958038795,244.830922997583,244.910793585687,244.990587322714,245.070321667805,
245.150014033113,245.229693251654,245.309369015444,245.389057047312,245.468773074424,
245.548576637355,245.628429362033,245.708395771684,245.749941540995,245.838109597556,
245.925942288221,246.013563054025,246.100834313321,246.163081868327),
 .UNSPECIFIED.);
#143=B_SPLINE_CURVE_WITH_KNOTS('',3,(#12788,#12789,#12790,#12791,#12792,
#12793,#12794,#12795,#12796,#12797),.UNSPECIFIED.,.F.,.F.,(4,1,1,1,1,1,
1,4),(246.163082073543,246.748925043194,247.747908545393,248.746892047592,
249.745875549791,250.74485905199,251.74384255419,252.446267380723),
 .UNSPECIFIED.);
#144=B_SPLINE_CURVE_WITH_KNOTS('',3,(#12799,#12800,#12801,#12802,#12803,
#12804,#12805,#12806,#12807,#12808,#12809,#12810,#12811,#12812,#12813,#12814,
#12815,#12816,#12817,#12818,#12819,#12820,#12821,#12822,#12823,#12824,#12825,
#12826,#12827,#12828,#12829,#12830,#12831,#12832,#12833,#12834,#12835,#12836,
#12837,#12838,#12839,#12840,#12841,#12842,#12843,#12844,#12845,#12846,#12847,
#12848,#12849,#12850,#12851,#12852,#12853,#12854,#12855,#12856,#12857,#12858,
#12859,#12860,#12861,#12862,#12863,#12864,#12865,#12866,#12867,#12868,#12869,
#12870,#12871,#12872,#12873,#12874,#12875,#12876,#12877,#12878,#12879,#12880,
#12881,#12882,#12883,#12884,#12885,#12886,#12887,#12888,#12889,#12890,#12891,
#12892,#12893,#12894,#12895,#12896,#12897,#12898,#12899,#12900,#12901,#12902,
#12903,#12904,#12905,#12906,#12907,#12908,#12909,#12910,#12911,#12912,#12913,
#12914,#12915,#12916,#12917,#12918,#12919,#12920,#12921,#12922,#12923,#12924,
#12925,#12926,#12927,#12928,#12929,#12930,#12931,#12932,#12933,#12934,#12935,
#12936,#12937,#12938,#12939,#12940,#12941,#12942,#12943,#12944,#12945,#12946,
#12947,#12948,#12949,#12950,#12951,#12952,#12953,#12954,#12955,#12956,#12957,
#12958,#12959,#12960,#12961,#12962,#12963,#12964,#12965,#12966,#12967,#12968,
#12969,#12970,#12971,#12972,#12973,#12974,#12975,#12976,#12977,#12978,#12979,
#12980,#12981,#12982,#12983,#12984,#12985,#12986,#12987,#12988,#12989,#12990,
#12991,#12992,#12993,#12994,#12995,#12996,#12997,#12998,#12999,#13000,#13001,
#13002,#13003,#13004,#13005,#13006,#13007,#13008,#13009,#13010,#13011,#13012,
#13013,#13014,#13015,#13016,#13017,#13018,#13019,#13020,#13021,#13022,#13023,
#13024,#13025,#13026,#13027,#13028,#13029,#13030,#13031,#13032,#13033,#13034,
#13035,#13036,#13037,#13038,#13039,#13040,#13041,#13042),.UNSPECIFIED.,
 .F.,.F.,(4,3,3,3,3,3,3,3,3,3,3,3,3,3,3,3,3,3,3,3,3,3,3,3,3,3,3,3,3,3,3,
3,3,3,3,3,3,3,3,3,3,3,3,3,3,3,3,3,3,3,3,3,3,3,3,3,3,3,3,3,3,3,3,3,3,3,3,
3,3,3,3,3,3,3,3,3,3,3,3,3,3,4),(252.446267557126,252.542602672679,252.642714364534,
252.742826056389,252.822791015176,252.902661603281,252.982455340307,253.062189685399,
253.141882050706,253.221561269247,253.301237033036,253.380925064903,253.460641092015,
253.540444654945,253.620297379623,253.700263789274,253.741809558588,253.821774517375,
253.90164510548,253.981438842507,254.061173187598,254.140865552905,254.220544771446,
254.300220535235,254.379908567103,254.459624594215,254.539428157145,254.619280881823,
254.699247291473,254.740793060787,254.820758019574,254.900628607679,254.980422344706,
255.060156689796,255.139849055103,255.219528273644,255.299204037433,255.378892069301,
255.458608096413,255.538411659343,255.618264384021,255.698230793671,255.739776562986,
255.819741521773,255.899612109878,255.979405846905,256.059140191996,256.138832557302,
256.218511775844,256.298187539633,256.377875571501,256.457591598612,256.537395161543,
256.617247886221,256.697214295871,256.738760065185,256.818725023972,256.898595612077,
256.978389349104,257.058123694196,257.137816059503,257.217495278044,257.297171041834,
257.376859073702,257.456575100814,257.536378663744,257.616231388422,257.696197798073,
257.737743567385,257.817605191863,257.897372494987,257.977063097636,258.056694559483,
258.136284392802,258.215861564402,258.295435783951,258.375022864638,258.454638624457,
258.534341873629,258.614095072686,258.693960146717,258.729452687902),
 .UNSPECIFIED.);
#145=B_SPLINE_CURVE_WITH_KNOTS('',3,(#13044,#13045,#13046,#13047,#13048,
#13049,#13050,#13051,#13052,#13053,#13054,#13055,#13056),.UNSPECIFIED.,
 .F.,.F.,(4,3,1,1,1,1,1,1,4),(258.729452687902,258.736727069584,259.735710571783,
260.734694073982,261.733677576181,262.73266107838,263.73164458058,264.730628082779,
265.012633520022),.UNSPECIFIED.);
#146=B_SPLINE_CURVE_WITH_KNOTS('',3,(#13058,#13059,#13060,#13061,#13062,
#13063,#13064,#13065,#13066,#13067,#13068,#13069,#13070,#13071,#13072,#13073,
#13074,#13075,#13076,#13077,#13078,#13079,#13080,#13081,#13082,#13083,#13084,
#13085,#13086,#13087,#13088,#13089,#13090,#13091,#13092,#13093,#13094,#13095,
#13096,#13097,#13098,#13099,#13100,#13101,#13102,#13103,#13104,#13105,#13106,
#13107,#13108,#13109,#13110,#13111,#13112,#13113,#13114,#13115,#13116,#13117,
#13118,#13119,#13120,#13121,#13122,#13123,#13124,#13125,#13126,#13127,#13128,
#13129,#13130,#13131,#13132,#13133,#13134,#13135,#13136,#13137,#13138,#13139,
#13140,#13141,#13142,#13143,#13144,#13145,#13146,#13147,#13148,#13149,#13150,
#13151,#13152,#13153,#13154,#13155,#13156,#13157,#13158,#13159,#13160,#13161,
#13162,#13163,#13164,#13165,#13166,#13167,#13168,#13169,#13170,#13171,#13172,
#13173,#13174,#13175,#13176,#13177,#13178,#13179,#13180,#13181,#13182,#13183,
#13184,#13185,#13186,#13187,#13188,#13189,#13190,#13191,#13192,#13193,#13194,
#13195,#13196,#13197,#13198,#13199,#13200,#13201,#13202,#13203,#13204,#13205,
#13206,#13207,#13208,#13209,#13210,#13211,#13212,#13213,#13214,#13215,#13216,
#13217,#13218,#13219,#13220,#13221,#13222,#13223,#13224,#13225,#13226,#13227,
#13228,#13229,#13230,#13231,#13232,#13233,#13234,#13235,#13236,#13237,#13238,
#13239,#13240,#13241,#13242,#13243,#13244,#13245,#13246,#13247,#13248,#13249,
#13250,#13251,#13252,#13253,#13254,#13255,#13256,#13257,#13258,#13259,#13260,
#13261,#13262,#13263,#13264,#13265,#13266,#13267,#13268,#13269,#13270,#13271,
#13272,#13273,#13274,#13275,#13276,#13277,#13278,#13279,#13280,#13281,#13282,
#13283,#13284,#13285,#13286,#13287,#13288,#13289,#13290,#13291,#13292,#13293,
#13294,#13295,#13296,#13297,#13298,#13299,#13300,#13301),.UNSPECIFIED.,
 .F.,.F.,(4,3,3,3,3,3,3,3,3,3,3,3,3,3,3,3,3,3,3,3,3,3,3,3,3,3,3,3,3,3,3,
3,3,3,3,3,3,3,3,3,3,3,3,3,3,3,3,3,3,3,3,3,3,3,3,3,3,3,3,3,3,3,3,3,3,3,3,
3,3,3,3,3,3,3,3,3,3,3,3,3,3,4),(265.012637995082,265.091707545985,265.171445550859,
265.250469629238,265.329495139418,265.408538307972,265.488806627223,265.567973819963,
265.64879270247,265.729611584978,265.809576543765,265.88944713187,265.969240868897,
266.048975213988,266.128667579295,266.208346797836,266.288022561625,266.367710593493,
266.447426620605,266.527230183535,266.607082908213,266.687049317863,266.728595087177,
266.808560045964,266.888430634069,266.968224371096,267.047958716187,267.127651081494,
267.207330300035,267.287006063824,267.366694095692,267.446410122803,267.526213685734,
267.606066410411,267.686032820062,267.727578589376,267.807543548163,267.887414136268,
267.967207873295,268.046942218386,268.126634583692,268.206313802234,268.285989566023,
268.36567759789,268.445393625002,268.525197187932,268.60504991261,268.68501632226,
268.726562091575,268.806527050362,268.886397638467,268.966191375494,269.045925720585,
269.125618085892,269.205297304433,269.284973068223,269.364661100091,269.444377127202,
269.524180690133,269.604033414811,269.683999824461,269.725545593775,269.805510552562,
269.885381140667,269.965174877694,270.044909222784,270.124601588092,270.204280806633,
270.283956570422,270.36364460229,270.443360629401,270.523164192332,270.603016917009,
270.68298332666,270.724529095974,270.806347626139,270.888056489702,270.969669026202,
271.051207595217,271.132651579875,271.214237441069,271.295823302262),
 .UNSPECIFIED.);
#147=B_SPLINE_CURVE_WITH_KNOTS('',3,(#13303,#13304,#13305,#13306,#13307,
#13308,#13309,#13310,#13311,#13312),.UNSPECIFIED.,.F.,.F.,(4,1,1,1,1,1,
1,4),(271.295828888875,271.723512598173,272.722496100372,273.721479602571,
274.72046310477,275.71944660697,276.718430109169,277.579008609441),
 .UNSPECIFIED.);
#148=B_SPLINE_CURVE_WITH_KNOTS('',3,(#13314,#13315,#13316,#13317,#13318,
#13319,#13320,#13321,#13322,#13323,#13324),.UNSPECIFIED.,.F.,.F.,(4,1,1,
1,1,1,1,1,4),(277.579008609441,277.717413611368,278.716397113567,279.715380615766,
280.714364117965,281.713347620165,282.712331122364,283.711314624563,283.862193916621),
 .UNSPECIFIED.);
#149=B_SPLINE_CURVE_WITH_KNOTS('',3,(#13326,#13327,#13328,#13329,#13330,
#13331,#13332,#13333,#13334,#13335),.UNSPECIFIED.,.F.,.F.,(4,1,1,1,1,1,
1,4),(283.862193916621,284.710298126762,285.709281628961,286.70826513116,
287.70724863336,288.706232135559,289.705215637758,290.14537443941),
 .UNSPECIFIED.);
#150=B_SPLINE_CURVE_WITH_KNOTS('',3,(#13337,#13338,#13339,#13340,#13341,
#13342,#13343,#13344,#13345,#13346,#13347,#13348,#13349,#13350,#13351,#13352,
#13353,#13354,#13355,#13356,#13357,#13358,#13359,#13360,#13361,#13362,#13363,
#13364,#13365,#13366,#13367,#13368,#13369,#13370,#13371,#13372,#13373,#13374,
#13375,#13376,#13377,#13378,#13379,#13380,#13381,#13382,#13383,#13384,#13385,
#13386,#13387,#13388,#13389,#13390,#13391,#13392,#13393,#13394,#13395,#13396,
#13397,#13398,#13399,#13400,#13401,#13402,#13403,#13404,#13405,#13406,#13407,
#13408,#13409,#13410,#13411,#13412,#13413,#13414,#13415,#13416,#13417,#13418,
#13419,#13420,#13421,#13422,#13423,#13424,#13425,#13426,#13427,#13428,#13429,
#13430,#13431,#13432,#13433,#13434,#13435,#13436,#13437,#13438,#13439,#13440,
#13441,#13442,#13443,#13444,#13445,#13446,#13447,#13448,#13449,#13450,#13451,
#13452,#13453,#13454,#13455,#13456,#13457,#13458,#13459,#13460,#13461,#13462,
#13463,#13464,#13465,#13466,#13467,#13468,#13469,#13470,#13471,#13472,#13473,
#13474,#13475,#13476,#13477,#13478,#13479,#13480,#13481,#13482,#13483,#13484,
#13485,#13486,#13487,#13488,#13489,#13490,#13491,#13492,#13493,#13494,#13495,
#13496,#13497,#13498,#13499,#13500,#13501,#13502,#13503,#13504,#13505,#13506,
#13507,#13508,#13509,#13510,#13511,#13512,#13513,#13514,#13515,#13516,#13517,
#13518,#13519,#13520,#13521,#13522,#13523,#13524,#13525,#13526,#13527,#13528,
#13529,#13530,#13531,#13532,#13533,#13534,#13535,#13536,#13537,#13538,#13539,
#13540,#13541,#13542,#13543,#13544,#13545,#13546,#13547,#13548,#13549,#13550,
#13551,#13552,#13553,#13554,#13555,#13556,#13557,#13558,#13559,#13560,#13561,
#13562,#13563,#13564,#13565,#13566,#13567,#13568,#13569,#13570,#13571,#13572,
#13573,#13574,#13575,#13576,#13577,#13578,#13579,#13580,#13581,#13582,#13583),
 .UNSPECIFIED.,.F.,.F.,(4,3,3,3,3,3,3,3,3,3,3,3,3,3,3,3,3,3,3,3,3,3,3,3,
3,3,3,3,3,3,3,3,3,3,3,3,3,3,3,3,3,3,3,3,3,3,3,3,3,3,3,3,3,3,3,3,3,3,3,3,
3,3,3,3,3,3,3,3,3,3,3,3,3,3,3,3,3,3,3,3,3,3,4),(290.1453792238,290.227064665826,
290.308797183107,290.390589213631,290.472514284967,290.55450951901,290.636657890419,
290.704199139957,290.784164098744,290.864034686849,290.943828423876,291.023562768967,
291.103255134273,291.182934352814,291.262610116604,291.342298148471,291.422014175583,
291.501817738513,291.581670463191,291.661636872841,291.703182642156,291.783147600943,
291.863018189048,291.942811926074,292.022546271165,292.102238636472,292.181917855013,
292.261593618802,292.34128165067,292.420997677781,292.500801240712,292.58065396539,
292.66062037504,292.702166144355,292.782131103142,292.862001691247,292.941795428274,
293.021529773366,293.101222138672,293.180901357214,293.260577121003,293.340265152871,
293.419981179983,293.499784742913,293.579637467591,293.659603877242,293.701149646555,
293.781114605343,293.860985193447,293.940778930474,294.020513275565,294.100205640872,
294.179884859414,294.259560623203,294.339248655071,294.418964682182,294.498768245113,
294.578620969791,294.658587379441,294.700133148754,294.780098107541,294.859968695646,
294.939762432672,295.019496777763,295.09918914307,295.178868361611,295.2585441254,
295.338232157267,295.417948184378,295.497751747308,295.577604471986,295.657570881637,
295.699116650953,295.77832390399,295.859603982364,295.938618021358,296.017578945768,
296.096503109002,296.179518464496,296.258435225525,296.337361479172,296.416332651885,
296.42856453098),.UNSPECIFIED.);
#151=B_SPLINE_CURVE_WITH_KNOTS('',3,(#13585,#13586,#13587,#13588,#13589,
#13590,#13591,#13592,#13593,#13594,#13595),.UNSPECIFIED.,.F.,.F.,(4,1,1,
1,1,1,1,1,4),(296.428568001001,296.698100153152,297.697083655351,298.69606715755,
299.69505065975,300.694034161949,301.693017664148,302.692001166347,302.711749838159),
 .UNSPECIFIED.);
#152=B_SPLINE_CURVE_WITH_KNOTS('',3,(#13597,#13598,#13599,#13600,#13601,
#13602,#13603,#13604,#13605,#13606,#13607,#13608,#13609,#13610,#13611,#13612,
#13613,#13614,#13615,#13616,#13617,#13618,#13619,#13620,#13621,#13622,#13623,
#13624,#13625,#13626,#13627,#13628,#13629,#13630,#13631,#13632,#13633,#13634,
#13635,#13636,#13637,#13638,#13639,#13640,#13641,#13642,#13643,#13644,#13645,
#13646,#13647,#13648,#13649,#13650,#13651,#13652,#13653,#13654,#13655,#13656,
#13657,#13658,#13659,#13660,#13661,#13662,#13663,#13664,#13665,#13666,#13667,
#13668,#13669,#13670,#13671,#13672,#13673,#13674,#13675,#13676,#13677,#13678,
#13679,#13680,#13681,#13682,#13683,#13684,#13685,#13686,#13687,#13688,#13689,
#13690,#13691,#13692,#13693,#13694,#13695,#13696,#13697,#13698,#13699,#13700,
#13701,#13702,#13703,#13704,#13705,#13706,#13707,#13708,#13709,#13710,#13711,
#13712,#13713,#13714,#13715,#13716,#13717,#13718,#13719,#13720,#13721,#13722,
#13723,#13724,#13725,#13726,#13727,#13728,#13729,#13730,#13731,#13732,#13733,
#13734,#13735,#13736,#13737,#13738,#13739,#13740,#13741,#13742,#13743,#13744,
#13745,#13746,#13747,#13748,#13749,#13750,#13751,#13752,#13753,#13754,#13755,
#13756,#13757,#13758,#13759,#13760,#13761,#13762,#13763,#13764,#13765,#13766,
#13767,#13768,#13769,#13770,#13771,#13772,#13773,#13774,#13775,#13776,#13777,
#13778,#13779,#13780,#13781,#13782,#13783,#13784,#13785,#13786,#13787,#13788,
#13789,#13790,#13791,#13792,#13793,#13794,#13795,#13796,#13797,#13798,#13799,
#13800,#13801,#13802,#13803,#13804,#13805,#13806,#13807,#13808,#13809,#13810,
#13811,#13812,#13813,#13814,#13815,#13816,#13817,#13818,#13819,#13820,#13821,
#13822,#13823,#13824,#13825,#13826,#13827,#13828,#13829,#13830,#13831,#13832,
#13833,#13834,#13835,#13836,#13837,#13838,#13839,#13840,#13841,#13842,#13843),
 .UNSPECIFIED.,.F.,.F.,(4,3,3,3,3,3,3,3,3,3,3,3,3,3,3,3,3,3,3,3,3,3,3,3,
3,3,3,3,3,3,3,3,3,3,3,3,3,3,3,3,3,3,3,3,3,3,3,3,3,3,3,3,3,3,3,3,3,3,3,3,
3,3,3,3,3,3,3,3,3,3,3,3,3,3,3,3,3,3,3,3,3,3,4),(302.711749838159,302.79144354471,
302.871043439066,302.950567294797,303.030032823128,303.112651803805,303.19206492816,
303.271476895875,303.350903657371,303.430361169323,303.509906619331,303.589504139084,
303.669209793545,303.690984668546,303.770949627333,303.850820215438,303.930613952464,
304.010348297555,304.090040662862,304.169719881403,304.249395645192,304.32908367706,
304.408799704171,304.488603267101,304.568455991779,304.64842240143,304.689968170745,
304.769933129532,304.849803717637,304.929597454664,305.009331799755,305.089024165062,
305.168703383603,305.248379147393,305.328067179261,305.407783206372,305.487586769303,
305.567439493981,305.647405903632,305.688951672945,305.768916631732,305.848787219837,
305.928580956864,306.008315301954,306.088007667261,306.167686885802,306.247362649592,
306.32705068146,306.406766708571,306.486570271502,306.566422996179,306.64638940583,
306.687935175144,306.767900133931,306.847770722036,306.927564459062,307.007298804153,
307.08699116946,307.166670388001,307.24634615179,307.326034183658,307.405750210769,
307.4855537737,307.565406498377,307.645372908027,307.686918677343,307.76688363613,
307.846754224235,307.926547961262,308.006282306353,308.085974671658,308.165653890199,
308.245329653989,308.325017685856,308.404733712967,308.484537275898,308.564390000576,
308.644356410227,308.685902179542,308.782302303291,308.878151809102,308.972997791882,
308.99493494478),.UNSPECIFIED.);
#153=B_SPLINE_CURVE_WITH_KNOTS('',3,(#13845,#13846,#13847,#13848,#13849,
#13850,#13851,#13852,#13853,#13854),.UNSPECIFIED.,.F.,.F.,(4,1,1,1,1,1,
1,4),(308.994935145339,309.684885681741,310.68386918394,311.682852686139,
312.681836188339,313.680819690538,314.679803192737,315.278120452519),
 .UNSPECIFIED.);
#154=B_SPLINE_CURVE_WITH_KNOTS('',3,(#13856,#13857,#13858,#13859,#13860,
#13861,#13862,#13863,#13864,#13865),.UNSPECIFIED.,.F.,.F.,(4,1,1,1,1,1,
1,4),(315.278120452519,315.678786694936,316.677770197135,317.676753699334,
318.675737201534,319.674720703733,320.673704205932,321.561305759698),
 .UNSPECIFIED.);
#155=B_SPLINE_CURVE_WITH_KNOTS('',3,(#13867,#13868,#13869,#13870,#13871,
#13872,#13873,#13874,#13875,#13876,#13877),.UNSPECIFIED.,.F.,.F.,(4,1,1,
1,1,1,1,1,4),(321.561305759698,321.672687708131,322.67167121033,323.67065471253,
324.669638214729,325.668621716928,326.667605219127,327.666588721326,327.844491066878),
 .UNSPECIFIED.);
#156=B_SPLINE_CURVE_WITH_KNOTS('',3,(#13879,#13880,#13881,#13882,#13883,
#13884,#13885,#13886,#13887,#13888,#13889,#13890,#13891,#13892,#13893,#13894,
#13895,#13896,#13897,#13898,#13899,#13900,#13901,#13902,#13903,#13904,#13905,
#13906,#13907,#13908,#13909,#13910,#13911,#13912,#13913,#13914,#13915,#13916,
#13917,#13918,#13919,#13920,#13921,#13922,#13923,#13924,#13925,#13926,#13927,
#13928,#13929,#13930,#13931,#13932,#13933,#13934,#13935,#13936,#13937,#13938,
#13939,#13940,#13941,#13942,#13943,#13944,#13945,#13946,#13947,#13948,#13949,
#13950,#13951,#13952,#13953,#13954,#13955,#13956,#13957,#13958,#13959,#13960,
#13961,#13962,#13963,#13964,#13965,#13966,#13967,#13968,#13969,#13970,#13971,
#13972,#13973,#13974,#13975,#13976,#13977,#13978,#13979,#13980,#13981,#13982,
#13983,#13984,#13985,#13986,#13987,#13988,#13989,#13990,#13991,#13992,#13993,
#13994,#13995,#13996,#13997,#13998,#13999,#14000,#14001,#14002,#14003,#14004,
#14005,#14006,#14007,#14008,#14009,#14010,#14011,#14012,#14013,#14014,#14015,
#14016,#14017,#14018,#14019,#14020,#14021,#14022,#14023,#14024,#14025,#14026,
#14027,#14028,#14029,#14030,#14031,#14032,#14033,#14034,#14035,#14036,#14037,
#14038,#14039,#14040,#14041,#14042,#14043,#14044,#14045,#14046,#14047,#14048,
#14049,#14050,#14051,#14052,#14053,#14054,#14055,#14056,#14057,#14058,#14059,
#14060,#14061,#14062,#14063,#14064,#14065,#14066,#14067,#14068,#14069,#14070,
#14071,#14072,#14073,#14074,#14075,#14076,#14077,#14078,#14079,#14080,#14081,
#14082,#14083,#14084,#14085,#14086,#14087,#14088,#14089,#14090,#14091,#14092,
#14093,#14094,#14095,#14096,#14097,#14098,#14099,#14100,#14101,#14102,#14103,
#14104,#14105,#14106,#14107,#14108,#14109,#14110,#14111,#14112,#14113,#14114,
#14115,#14116,#14117,#14118,#14119,#14120,#14121,#14122,#14123,#14124,#14125),
 .UNSPECIFIED.,.F.,.F.,(4,3,3,3,3,3,3,3,3,3,3,3,3,3,3,3,3,3,3,3,3,3,3,3,
3,3,3,3,3,3,3,3,3,3,3,3,3,3,3,3,3,3,3,3,3,3,3,3,3,3,3,3,3,3,3,3,3,3,3,3,
3,3,3,3,3,3,3,3,3,3,3,3,3,3,3,3,3,3,3,3,3,3,4),(327.844491066878,327.923144699921,
328.001729551288,328.080264002823,328.15877503681,328.237276674429,328.315785478742,
328.39431801673,328.472932791003,328.551594499629,328.630365503201,328.665572223525,
328.745537182313,328.825407770417,328.905201507444,328.984935852536,329.064628217843,
329.144307436384,329.223983200174,329.303671232042,329.383387259154,329.463190822085,
329.543043546763,329.623009956414,329.664555725725,329.744520684512,329.824391272617,
329.904185009644,329.983919354735,330.063611720042,330.143290938583,330.222966702372,
330.30265473424,330.382370761351,330.462174324282,330.542027048959,330.62199345861,
330.663539227924,330.743504186711,330.823374774816,330.903168511842,330.982902856933,
331.062595222239,331.142274440781,331.22195020457,331.301638236437,331.381354263548,
331.461157826479,331.541010551156,331.620976960807,331.662522730123,331.74248768891,
331.822358277015,331.902152014042,331.981886359133,332.06157872444,332.141257942982,
332.220933706771,332.300621738639,332.380337765751,332.460141328681,332.539994053359,
332.61996046301,332.661506232322,332.741471191109,332.821341779214,332.901135516241,
332.980869861331,333.060562226638,333.140241445179,333.219917208968,333.299605240835,
333.379321267947,333.459124830878,333.538977555556,333.618943965207,333.660489734521,
333.74589133337,333.831132944262,333.916147981114,334.001024756027,334.085707551949,
334.127676197482),.UNSPECIFIED.);
#157=B_SPLINE_CURVE_WITH_KNOTS('',3,(#14127,#14128,#14129,#14130,#14131,
#14132,#14133,#14134,#14135,#14136),.UNSPECIFIED.,.F.,.F.,(4,1,1,1,1,1,
1,4),(334.127676374057,334.65947323672,335.65845673892,336.657440241119,
337.656423743318,338.655407245517,339.654390747716,340.410861681237),
 .UNSPECIFIED.);
#158=B_SPLINE_CURVE_WITH_KNOTS('',3,(#14138,#14139,#14140,#14141,#14142,
#14143,#14144,#14145,#14146,#14147,#14148,#14149,#14150,#14151,#14152,#14153,
#14154,#14155,#14156,#14157,#14158,#14159,#14160,#14161,#14162,#14163,#14164,
#14165,#14166,#14167,#14168,#14169,#14170,#14171,#14172,#14173,#14174,#14175,
#14176,#14177,#14178,#14179,#14180,#14181,#14182,#14183,#14184,#14185,#14186,
#14187,#14188,#14189,#14190,#14191,#14192,#14193,#14194,#14195,#14196,#14197,
#14198,#14199,#14200,#14201,#14202,#14203,#14204,#14205,#14206,#14207,#14208,
#14209,#14210,#14211,#14212,#14213,#14214,#14215,#14216,#14217,#14218,#14219,
#14220,#14221,#14222,#14223,#14224,#14225,#14226,#14227,#14228,#14229,#14230,
#14231,#14232,#14233,#14234,#14235,#14236,#14237,#14238,#14239,#14240,#14241,
#14242,#14243,#14244,#14245,#14246,#14247,#14248,#14249,#14250,#14251,#14252,
#14253,#14254,#14255,#14256,#14257,#14258,#14259,#14260,#14261,#14262,#14263,
#14264,#14265,#14266,#14267,#14268,#14269,#14270,#14271,#14272,#14273,#14274,
#14275,#14276,#14277,#14278,#14279,#14280,#14281,#14282,#14283,#14284,#14285,
#14286,#14287,#14288,#14289,#14290,#14291,#14292,#14293,#14294,#14295,#14296,
#14297,#14298,#14299,#14300,#14301,#14302,#14303,#14304,#14305,#14306,#14307,
#14308,#14309,#14310,#14311,#14312,#14313,#14314,#14315,#14316,#14317,#14318,
#14319,#14320,#14321,#14322,#14323,#14324,#14325,#14326,#14327,#14328,#14329,
#14330,#14331,#14332,#14333,#14334,#14335,#14336,#14337,#14338,#14339,#14340,
#14341,#14342,#14343,#14344,#14345,#14346,#14347,#14348,#14349,#14350,#14351,
#14352,#14353,#14354,#14355,#14356,#14357,#14358,#14359,#14360,#14361,#14362,
#14363,#14364,#14365,#14366,#14367,#14368,#14369,#14370,#14371,#14372,#14373,
#14374,#14375,#14376,#14377,#14378,#14379,#14380,#14381,#14382,#14383,#14384),
 .UNSPECIFIED.,.F.,.F.,(4,3,3,3,3,3,3,3,3,3,3,3,3,3,3,3,3,3,3,3,3,3,3,3,
3,3,3,3,3,3,3,3,3,3,3,3,3,3,3,3,3,3,3,3,3,3,3,3,3,3,3,3,3,3,3,3,3,3,3,3,
3,3,3,3,3,3,3,3,3,3,3,3,3,3,3,3,3,3,3,3,3,3,4),(340.410861744717,340.5143839423,
340.620403447411,340.653374249915,340.733339208702,340.813209796807,340.893003533834,
340.972737878925,341.052430244232,341.132109462773,341.211785226562,341.29147325843,
341.371189285542,341.450992848473,341.530845573151,341.610811982801,341.652357752114,
341.732322710902,341.812193299006,341.891987036033,341.971721381125,342.051413746432,
342.131092964973,342.210768728762,342.29045676063,342.370172787742,342.449976350673,
342.529829075351,342.609795485001,342.651341254314,342.731306213101,342.811176801206,
342.890970538233,342.970704883324,343.050397248631,343.130076467172,343.209752230961,
343.289440262829,343.369156289941,343.448959852871,343.528812577549,343.6087789872,
343.650324756513,343.7302897153,343.810160303405,343.889954040431,343.969688385522,
344.049380750829,344.12905996937,344.208735733159,344.288423765027,344.368139792138,
344.447943355068,344.527796079746,344.607762489396,344.649308258712,344.729273217499,
344.809143805604,344.888937542631,344.968671887722,345.048364253029,345.12804347157,
345.207719235359,345.287407267227,345.367123294339,345.446926857269,345.526779581947,
345.606745991598,345.648291760911,345.728256719698,345.808127307803,345.88792104483,
345.967655389921,346.047347755228,346.127026973769,346.206702737558,346.286390769426,
346.366106796537,346.445910359467,346.525763084145,346.605729493796,346.64727526311,
346.694046988416),.UNSPECIFIED.);
#159=B_SPLINE_CURVE_WITH_KNOTS('',3,(#14386,#14387,#14388,#14389,#14390,
#14391,#14392,#14393,#14394,#14395),.UNSPECIFIED.,.F.,.F.,(4,1,1,1,1,1,
1,4),(346.694053119753,347.64625876531,348.645242267509,349.644225769708,
350.643209271907,351.642192774106,352.641176276305,352.977224842988),
 .UNSPECIFIED.);
#160=B_SPLINE_CURVE_WITH_KNOTS('',3,(#14397,#14398,#14399,#14400,#14401,
#14402,#14403,#14404,#14405,#14406,#14407,#14408,#14409,#14410,#14411,#14412,
#14413,#14414,#14415,#14416,#14417,#14418,#14419,#14420,#14421,#14422,#14423,
#14424,#14425,#14426,#14427,#14428,#14429,#14430,#14431,#14432,#14433,#14434,
#14435,#14436,#14437,#14438,#14439,#14440,#14441,#14442,#14443,#14444,#14445,
#14446,#14447,#14448,#14449,#14450,#14451,#14452,#14453,#14454,#14455,#14456,
#14457,#14458,#14459,#14460,#14461,#14462,#14463,#14464,#14465,#14466,#14467,
#14468,#14469,#14470,#14471,#14472,#14473,#14474,#14475,#14476,#14477,#14478,
#14479,#14480,#14481,#14482,#14483,#14484,#14485,#14486,#14487,#14488,#14489,
#14490,#14491,#14492,#14493,#14494,#14495,#14496,#14497,#14498,#14499,#14500,
#14501,#14502,#14503,#14504,#14505,#14506,#14507,#14508,#14509,#14510,#14511,
#14512,#14513,#14514,#14515,#14516,#14517,#14518,#14519,#14520,#14521,#14522,
#14523,#14524,#14525,#14526,#14527,#14528,#14529,#14530,#14531,#14532,#14533,
#14534,#14535,#14536,#14537,#14538,#14539,#14540,#14541,#14542,#14543,#14544,
#14545,#14546,#14547,#14548,#14549,#14550,#14551,#14552,#14553,#14554,#14555,
#14556,#14557,#14558,#14559,#14560,#14561,#14562,#14563,#14564,#14565,#14566,
#14567,#14568,#14569,#14570,#14571,#14572,#14573,#14574,#14575,#14576,#14577,
#14578,#14579,#14580,#14581,#14582,#14583,#14584,#14585,#14586,#14587,#14588,
#14589,#14590,#14591,#14592,#14593,#14594,#14595,#14596,#14597,#14598,#14599,
#14600,#14601,#14602,#14603,#14604,#14605,#14606,#14607,#14608,#14609,#14610,
#14611,#14612,#14613,#14614,#14615,#14616,#14617,#14618,#14619,#14620,#14621,
#14622,#14623,#14624,#14625,#14626,#14627,#14628,#14629,#14630,#14631,#14632,
#14633,#14634,#14635,#14636,#14637,#14638,#14639,#14640,#14641,#14642,#14643),
 .UNSPECIFIED.,.F.,.F.,(4,3,3,3,3,3,3,3,3,3,3,3,3,3,3,3,3,3,3,3,3,3,3,3,
3,3,3,3,3,3,3,3,3,3,3,3,3,3,3,3,3,3,3,3,3,3,3,3,3,3,3,3,3,3,3,3,3,3,3,3,
3,3,3,3,3,3,3,3,3,3,3,3,3,3,3,3,3,3,3,3,3,3,4),(352.977232295596,353.06009823096,
353.139757082557,353.219420900244,353.299105357425,353.378826136887,353.458642309883,
353.538514879143,353.618501117166,353.640159778504,353.720124737292,353.799995325396,
353.879789062424,353.959523407515,354.039215772822,354.118894991363,354.198570755153,
354.278258787021,354.357974814133,354.437778377064,354.517631101742,354.597597511393,
354.639143280704,354.719108239491,354.798978827596,354.878772564623,354.958506909714,
355.038199275021,355.117878493562,355.197554257351,355.277242289219,355.35695831633,
355.436761879261,355.516614603939,355.596581013589,355.638126782903,355.71809174169,
355.797962329795,355.877756066821,355.957490411912,356.037182777219,356.11686199576,
356.196537759549,356.276225791417,356.355941818528,356.435745381459,356.515598106136,
356.595564515787,356.637110285102,356.717075243889,356.796945831994,356.876739569021,
356.956473914113,357.03616627942,357.115845497961,357.19552126175,357.275209293618,
357.35492532073,357.43472888366,357.514581608338,357.594548017989,357.636093787301,
357.716058746088,357.795929334193,357.875723071219,357.95545741631,358.035149781616,
358.114829000158,358.194504763947,358.274192795815,358.353908822926,358.433712385856,
358.513565110534,358.593531520184,358.6350772895,358.715679342861,358.796183603853,
358.876605222163,358.956959293157,359.03725629139,359.117519135194,359.197772296352,
359.260417602776),.UNSPECIFIED.);
#161=B_SPLINE_CURVE_WITH_KNOTS('',3,(#14645,#14646,#14647,#14648,#14649,
#14650,#14651,#14652,#14653,#14654),.UNSPECIFIED.,.F.,.F.,(4,1,1,1,1,1,
1,4),(359.260425213007,359.634060791699,360.633044293899,361.632027796098,
362.631011298297,363.629994800496,364.628978302695,365.543602909955),
 .UNSPECIFIED.);
#162=B_SPLINE_CURVE_WITH_KNOTS('',3,(#14656,#14657,#14658,#14659,#14660,
#14661,#14662,#14663,#14664,#14665,#14666,#14667),.UNSPECIFIED.,.F.,.F.,
(4,2,1,1,1,1,1,1,4),(365.543602909955,365.627961804895,366.626945307094,
367.625928809293,368.624912311492,369.623895813691,370.62287931589,371.62186281809,
371.826788217135),.UNSPECIFIED.);
#163=B_SPLINE_CURVE_WITH_KNOTS('',3,(#14669,#14670,#14671,#14672,#14673,
#14674,#14675,#14676,#14677,#14678,#14679,#14680,#14681,#14682,#14683,#14684,
#14685,#14686,#14687,#14688,#14689,#14690,#14691,#14692,#14693,#14694,#14695,
#14696,#14697,#14698,#14699,#14700,#14701,#14702,#14703,#14704,#14705,#14706,
#14707,#14708,#14709,#14710,#14711,#14712,#14713,#14714,#14715,#14716,#14717,
#14718,#14719,#14720,#14721,#14722,#14723,#14724,#14725,#14726,#14727,#14728,
#14729,#14730,#14731,#14732,#14733,#14734,#14735,#14736,#14737,#14738,#14739,
#14740,#14741,#14742,#14743,#14744,#14745,#14746,#14747,#14748,#14749,#14750,
#14751,#14752,#14753,#14754,#14755,#14756,#14757,#14758,#14759,#14760,#14761,
#14762,#14763,#14764,#14765,#14766,#14767,#14768,#14769,#14770,#14771,#14772,
#14773,#14774,#14775,#14776,#14777,#14778,#14779,#14780,#14781,#14782,#14783,
#14784,#14785,#14786,#14787,#14788,#14789,#14790,#14791,#14792,#14793,#14794,
#14795,#14796,#14797,#14798,#14799,#14800,#14801,#14802,#14803,#14804,#14805,
#14806,#14807,#14808,#14809,#14810,#14811,#14812,#14813,#14814,#14815,#14816,
#14817,#14818,#14819,#14820,#14821,#14822,#14823,#14824,#14825,#14826,#14827,
#14828,#14829,#14830,#14831,#14832,#14833,#14834,#14835,#14836,#14837,#14838,
#14839,#14840,#14841,#14842,#14843,#14844,#14845,#14846,#14847,#14848,#14849,
#14850,#14851,#14852,#14853,#14854,#14855,#14856,#14857,#14858,#14859,#14860,
#14861,#14862,#14863,#14864,#14865,#14866,#14867,#14868,#14869,#14870,#14871,
#14872,#14873,#14874,#14875,#14876,#14877,#14878,#14879,#14880,#14881,#14882,
#14883,#14884,#14885,#14886,#14887,#14888,#14889,#14890,#14891,#14892,#14893,
#14894,#14895,#14896,#14897,#14898,#14899,#14900,#14901,#14902,#14903,#14904,
#14905,#14906,#14907,#14908,#14909,#14910,#14911,#14912),.UNSPECIFIED.,
 .F.,.F.,(4,3,3,3,3,3,3,3,3,3,3,3,3,3,3,3,3,3,3,3,3,3,3,3,3,3,3,3,3,3,3,
3,3,3,3,3,3,3,3,3,3,3,3,3,3,3,3,3,3,3,3,3,3,3,3,3,3,3,3,3,3,3,3,3,3,3,3,
3,3,3,3,3,3,3,3,3,3,3,3,3,3,4),(371.826788217135,371.905463396283,371.984076702167,
372.063672904432,372.142227785294,372.220779624991,372.299344958611,372.37972029903,
372.458401859117,372.539624089703,372.620846320289,372.700811279076,372.780681867181,
372.860475604208,372.940209949299,373.019902314605,373.099581533147,373.179257296936,
373.258945328804,373.338661355915,373.418464918845,373.498317643523,373.578284053174,
373.619829822488,373.699794781275,373.77966536938,373.859459106407,373.939193451498,
374.018885816805,374.098565035346,374.178240799135,374.257928831003,374.337644858115,
374.417448421046,374.497301145723,374.577267555374,374.618813324687,374.698778283474,
374.778648871579,374.858442608606,374.938176953697,375.017869319004,375.097548537545,
375.177224301335,375.256912333203,375.336628360314,375.416431923245,375.496284647923,
375.576251057573,375.617796826886,375.697761785673,375.777632373778,375.857426110805,
375.937160455896,376.016852821203,376.096532039744,376.176207803533,376.255895835401,
376.335611862512,376.415415425443,376.49526815012,376.575234559771,376.616780329085,
376.696745287872,376.776615875977,376.856409613004,376.936143958095,377.015836323402,
377.095515541943,377.175191305732,377.2548793376,377.334595364712,377.414398927642,
377.49425165232,377.57421806197,377.615763831284,377.700046285104,377.784187229288,
377.868135337036,377.951969959806,378.035648096222,378.109973524199),
 .UNSPECIFIED.);
#164=B_SPLINE_CURVE_WITH_KNOTS('',3,(#14914,#14915,#14916,#14917,#14918,
#14919,#14920,#14921,#14922,#14923,#14924,#14925,#14926,#14927,#14928,#14929,
#14930,#14931,#14932,#14933,#14934,#14935,#14936,#14937,#14938,#14939,#14940,
#14941,#14942,#14943,#14944,#14945,#14946,#14947,#14948,#14949,#14950,#14951,
#14952,#14953,#14954,#14955,#14956,#14957,#14958,#14959,#14960,#14961,#14962,
#14963,#14964,#14965,#14966,#14967,#14968,#14969,#14970,#14971,#14972,#14973,
#14974,#14975,#14976,#14977,#14978,#14979,#14980,#14981,#14982,#14983,#14984,
#14985,#14986,#14987,#14988,#14989,#14990,#14991,#14992,#14993,#14994,#14995,
#14996,#14997,#14998,#14999,#15000,#15001,#15002,#15003,#15004,#15005,#15006,
#15007,#15008,#15009,#15010,#15011,#15012,#15013,#15014,#15015,#15016,#15017,
#15018,#15019,#15020,#15021,#15022,#15023,#15024,#15025,#15026,#15027,#15028,
#15029,#15030,#15031,#15032,#15033,#15034,#15035,#15036,#15037,#15038,#15039,
#15040,#15041,#15042,#15043,#15044,#15045,#15046,#15047,#15048,#15049,#15050,
#15051,#15052,#15053,#15054,#15055,#15056,#15057,#15058,#15059,#15060,#15061,
#15062,#15063,#15064,#15065,#15066,#15067,#15068,#15069,#15070,#15071,#15072,
#15073,#15074,#15075,#15076,#15077,#15078,#15079,#15080,#15081,#15082,#15083,
#15084,#15085,#15086,#15087,#15088,#15089,#15090,#15091,#15092,#15093,#15094,
#15095,#15096,#15097,#15098,#15099,#15100,#15101,#15102,#15103,#15104,#15105,
#15106,#15107,#15108,#15109,#15110,#15111,#15112,#15113,#15114,#15115,#15116,
#15117,#15118,#15119,#15120,#15121,#15122,#15123,#15124,#15125,#15126,#15127,
#15128,#15129,#15130,#15131,#15132,#15133,#15134,#15135,#15136,#15137,#15138,
#15139,#15140,#15141,#15142,#15143,#15144,#15145,#15146,#15147,#15148,#15149,
#15150,#15151,#15152,#15153,#15154,#15155,#15156,#15157),.UNSPECIFIED.,
 .F.,.F.,(4,3,3,3,3,3,3,3,3,3,3,3,3,3,3,3,3,3,3,3,3,3,3,3,3,3,3,3,3,3,3,
3,3,3,3,3,3,3,3,3,3,3,3,3,3,3,3,3,3,3,3,3,3,3,3,3,3,3,3,3,3,3,3,3,3,3,3,
3,3,3,3,3,3,3,3,3,3,3,3,3,3,4),(378.109973524314,378.193253743236,378.276632185242,
378.361160972303,378.444821525,378.529784429242,378.614747333484,378.694712292271,
378.774582880375,378.854376617402,378.934110962492,379.013803327799,379.09348254634,
379.173158310129,379.252846341996,379.332562369107,379.412365932038,379.492218656715,
379.572185066365,379.613730835683,379.69369579447,379.773566382575,379.853360119602,
379.933094464692,380.012786829999,380.092466048541,380.17214181233,380.251829844198,
380.331545871309,380.411349434239,380.491202158917,380.571168568568,380.612714337882,
380.692679296669,380.772549884774,380.852343621801,380.932077966892,381.011770332199,
381.09144955074,381.171125314529,381.250813346397,381.330529373509,381.41033293644,
381.490185661118,381.570152070768,381.611697840081,381.691662798868,381.771533386973,
381.851327123999,381.93106146909,382.010753834398,382.090433052939,382.170108816728,
382.249796848595,382.329512875706,382.409316438637,382.489169163314,382.569135572965,
382.61068134228,382.690646301067,382.770516889172,382.850310626199,382.93004497129,
383.009737336597,383.089416555138,383.169092318928,383.248780350796,383.328496377907,
383.408299940838,383.488152665516,383.568119075167,383.60966484448,383.688530682252,
383.767301609312,383.845983160986,383.924614195004,384.00321127053,384.081790918647,
384.160397349559,384.239014939738,384.317705749996,384.393158831494),
 .UNSPECIFIED.);
#165=B_SPLINE_CURVE_WITH_KNOTS('',3,(#15159,#15160,#15161,#15162,#15163,
#15164,#15165,#15166,#15167,#15168,#15169),.UNSPECIFIED.,.F.,.F.,(4,1,1,
1,1,1,1,1,4),(384.393158831494,384.608648346679,385.607631848878,386.606615351077,
387.605598853276,388.604582355475,389.603565857674,390.602549359874,390.676344138673),
 .UNSPECIFIED.);
#166=B_SPLINE_CURVE_WITH_KNOTS('',3,(#15171,#15172,#15173,#15174,#15175,
#15176,#15177,#15178,#15179,#15180),.UNSPECIFIED.,.F.,.F.,(4,1,1,1,1,1,
1,4),(390.676344138673,391.601532862073,392.600516364272,393.599499866471,
394.59848336867,395.597466870869,396.596450373069,396.959529445853),
 .UNSPECIFIED.);
#167=B_SPLINE_CURVE_WITH_KNOTS('',3,(#15182,#15183,#15184,#15185,#15186,
#15187,#15188,#15189,#15190,#15191),.UNSPECIFIED.,.F.,.F.,(4,1,1,1,1,1,
1,4),(396.959529445853,397.595433875268,398.594417377467,399.593400879666,
400.592384381865,401.591367884064,402.590351386264,403.242714753032),
 .UNSPECIFIED.);
#168=B_SPLINE_CURVE_WITH_KNOTS('',3,(#15193,#15194,#15195,#15196,#15197,
#15198,#15199,#15200,#15201,#15202,#15203,#15204,#15205,#15206,#15207,#15208,
#15209,#15210,#15211,#15212,#15213,#15214,#15215,#15216,#15217,#15218,#15219,
#15220,#15221,#15222,#15223,#15224,#15225,#15226,#15227,#15228,#15229,#15230,
#15231,#15232,#15233,#15234,#15235,#15236,#15237,#15238,#15239,#15240,#15241,
#15242,#15243,#15244,#15245,#15246,#15247,#15248,#15249,#15250,#15251,#15252,
#15253,#15254,#15255,#15256,#15257,#15258,#15259,#15260,#15261,#15262,#15263,
#15264,#15265,#15266,#15267,#15268,#15269,#15270,#15271,#15272,#15273,#15274,
#15275,#15276,#15277,#15278,#15279,#15280,#15281,#15282,#15283,#15284,#15285,
#15286,#15287,#15288,#15289,#15290,#15291,#15292,#15293,#15294,#15295,#15296,
#15297,#15298,#15299,#15300,#15301,#15302,#15303,#15304,#15305,#15306,#15307,
#15308,#15309,#15310,#15311,#15312,#15313,#15314,#15315,#15316,#15317,#15318,
#15319,#15320,#15321,#15322,#15323,#15324,#15325,#15326,#15327,#15328,#15329,
#15330,#15331,#15332,#15333,#15334,#15335,#15336,#15337,#15338,#15339,#15340,
#15341,#15342,#15343,#15344,#15345,#15346,#15347,#15348,#15349,#15350,#15351,
#15352,#15353,#15354,#15355,#15356,#15357,#15358,#15359,#15360,#15361,#15362,
#15363,#15364,#15365,#15366,#15367,#15368,#15369,#15370,#15371,#15372,#15373,
#15374,#15375,#15376,#15377,#15378,#15379,#15380,#15381,#15382,#15383,#15384,
#15385,#15386,#15387,#15388,#15389,#15390,#15391,#15392,#15393,#15394,#15395,
#15396,#15397,#15398,#15399,#15400,#15401,#15402,#15403,#15404,#15405,#15406,
#15407,#15408,#15409,#15410,#15411,#15412,#15413,#15414,#15415,#15416,#15417,
#15418,#15419,#15420,#15421,#15422,#15423,#15424,#15425,#15426,#15427,#15428,
#15429,#15430,#15431,#15432,#15433,#15434,#15435,#15436),.UNSPECIFIED.,
 .F.,.F.,(4,3,3,3,3,3,3,3,3,3,3,3,3,3,3,3,3,3,3,3,3,3,3,3,3,3,3,3,3,3,3,
3,3,3,3,3,3,3,3,3,3,3,3,3,3,3,3,3,3,3,3,3,3,3,3,3,3,3,3,3,3,3,3,3,3,3,3,
3,3,3,3,3,3,3,3,3,3,3,3,3,3,4),(403.24271487461,403.334441411454,403.426617865222,
403.519381278125,403.589334888463,403.66929984725,403.749170435354,403.82896417238,
403.908698517471,403.988390882778,404.068070101318,404.147745865107,404.227433896974,
404.307149924086,404.386953487016,404.466806211693,404.546772621343,404.588318390662,
404.668283349449,404.748153937554,404.827947674581,404.907682019672,404.987374384979,
405.06705360352,405.146729367309,405.226417399177,405.306133426288,405.385936989219,
405.465789713897,405.545756123547,405.587301892861,405.667266851648,405.747137439753,
405.82693117678,405.906665521871,405.986357887178,406.06603710572,406.145712869509,
406.225400901377,406.305116928489,406.384920491419,406.464773216097,406.544739625748,
406.58628539506,406.666250353847,406.746120941952,406.825914678978,406.905649024069,
406.985341389376,407.065020607917,407.144696371706,407.224384403574,407.304100430685,
407.383903993615,407.463756718293,407.543723127943,407.585268897259,407.665233856046,
407.745104444151,407.824898181178,407.904632526269,407.984324891576,408.064004110118,
408.143679873907,408.223367905775,408.303083932887,408.382887495817,408.462740220496,
408.542706630146,408.584252399459,408.663535534452,408.742724767276,408.821838218944,
408.900893942308,408.979915849117,409.058921070256,409.137925862554,409.216946480107,
409.296044176676,409.375181216383,409.454434737698,409.525900060212),
 .UNSPECIFIED.);
#169=B_SPLINE_CURVE_WITH_KNOTS('',3,(#15438,#15439,#15440,#15441,#15442,
#15443,#15444,#15445,#15446,#15447,#15448,#15449),.UNSPECIFIED.,.F.,.F.,
(4,2,1,1,1,1,1,1,4),(409.525900060212,409.583235901658,410.582219403857,
411.581202906056,412.580186408255,413.579169910454,414.578153412654,415.577136914853,
415.809085367392),.UNSPECIFIED.);
#170=B_SPLINE_CURVE_WITH_KNOTS('',3,(#15451,#15452,#15453,#15454,#15455,
#15456,#15457,#15458,#15459,#15460),.UNSPECIFIED.,.F.,.F.,(4,1,1,1,1,1,
1,4),(415.809085367392,416.576120417052,417.575103919251,418.57408742145,
419.573070923649,420.572054425849,421.571037928048,422.092270674571),
 .UNSPECIFIED.);
#171=B_SPLINE_CURVE_WITH_KNOTS('',3,(#15462,#15463,#15464,#15465,#15466,
#15467,#15468,#15469,#15470,#15471),.UNSPECIFIED.,.F.,.F.,(4,1,1,1,1,1,
1,4),(422.092270674571,422.570021430247,423.569004932446,424.567988434645,
425.566971936844,426.565955439044,427.564938941243,428.375451647274),
 .UNSPECIFIED.);
#172=B_SPLINE_CURVE_WITH_KNOTS('',3,(#15473,#15474,#15475,#15476,#15477,
#15478,#15479,#15480,#15481,#15482,#15483,#15484,#15485,#15486,#15487,#15488,
#15489,#15490,#15491,#15492,#15493,#15494,#15495,#15496,#15497,#15498,#15499,
#15500,#15501,#15502,#15503,#15504,#15505,#15506,#15507,#15508,#15509,#15510,
#15511,#15512,#15513,#15514,#15515,#15516,#15517,#15518,#15519,#15520,#15521,
#15522,#15523,#15524,#15525,#15526,#15527,#15528,#15529,#15530,#15531,#15532,
#15533,#15534,#15535,#15536,#15537,#15538,#15539,#15540,#15541,#15542,#15543,
#15544,#15545,#15546,#15547,#15548,#15549,#15550,#15551,#15552,#15553,#15554,
#15555,#15556,#15557,#15558,#15559,#15560,#15561,#15562,#15563,#15564,#15565,
#15566,#15567,#15568,#15569,#15570,#15571,#15572,#15573,#15574,#15575,#15576,
#15577,#15578,#15579,#15580,#15581,#15582,#15583,#15584,#15585,#15586,#15587,
#15588,#15589,#15590,#15591,#15592,#15593,#15594,#15595,#15596,#15597,#15598,
#15599,#15600,#15601,#15602,#15603,#15604,#15605,#15606,#15607,#15608,#15609,
#15610,#15611,#15612,#15613,#15614,#15615,#15616,#15617,#15618,#15619,#15620,
#15621,#15622,#15623,#15624,#15625,#15626,#15627,#15628,#15629,#15630,#15631,
#15632,#15633,#15634,#15635,#15636,#15637,#15638,#15639,#15640,#15641,#15642,
#15643,#15644,#15645,#15646,#15647,#15648,#15649,#15650,#15651,#15652,#15653,
#15654,#15655,#15656,#15657,#15658,#15659,#15660,#15661,#15662,#15663,#15664,
#15665,#15666,#15667,#15668,#15669,#15670,#15671,#15672,#15673,#15674,#15675,
#15676,#15677,#15678,#15679,#15680,#15681,#15682,#15683,#15684,#15685,#15686,
#15687,#15688,#15689,#15690,#15691,#15692,#15693,#15694,#15695,#15696,#15697,
#15698,#15699,#15700,#15701,#15702,#15703,#15704,#15705,#15706,#15707,#15708,
#15709,#15710,#15711,#15712,#15713,#15714,#15715,#15716),.UNSPECIFIED.,
 .F.,.F.,(4,3,3,3,3,3,3,3,3,3,3,3,3,3,3,3,3,3,3,3,3,3,3,3,3,3,3,3,3,3,3,
3,3,3,3,3,3,3,3,3,3,3,3,3,3,3,3,3,3,3,3,3,3,3,3,3,3,3,3,3,3,3,3,3,3,3,3,
3,3,3,3,3,3,3,3,3,3,3,3,3,3,4),(428.375455981751,428.493703066263,428.563922443442,
428.64388740223,428.723757990335,428.803551727362,428.883286072453,428.962978437761,
429.042657656303,429.122333420092,429.202021451961,429.281737479072,429.361541042003,
429.441393766682,429.521360176333,429.562905945641,429.642870904428,429.722741492533,
429.802535229559,429.88226957465,429.961961939957,430.041641158498,430.121316922287,
430.201004954155,430.280720981267,430.360524544197,430.440377268875,430.520343678525,
430.56188944784,430.641854406627,430.721724994732,430.801518731758,430.881253076849,
430.960945442156,431.040624660697,431.120300424486,431.199988456354,431.279704483466,
431.359508046396,431.439360771074,431.519327180724,431.560872950039,431.640837908826,
431.720708496931,431.800502233958,431.880236579049,431.959928944356,432.039608162897,
432.119283926686,432.198971958554,432.278687985665,432.358491548595,432.438344273273,
432.518310682924,432.559856452238,432.639821411026,432.71969199913,432.799485736157,
432.879220081249,432.958912446556,433.038591665097,433.118267428886,433.197955460754,
433.277671487866,433.357475050797,433.437327775475,433.517294185126,433.558839954438,
433.638804913225,433.71867550133,433.798469238357,433.878203583448,433.957895948755,
434.037575167297,434.117250931086,434.196938962954,434.276654990065,434.356458552996,
434.436311277674,434.516277687325,434.557823456637,434.65864128893),
 .UNSPECIFIED.);
#173=B_SPLINE_CURVE_WITH_KNOTS('',3,(#15718,#15719,#15720,#15721,#15722,
#15723,#15724,#15725,#15726,#15727),.UNSPECIFIED.,.F.,.F.,(4,1,1,1,1,1,
1,4),(434.658650333521,435.556806958836,436.555790461035,437.554773963234,
438.553757465434,439.552740967633,440.551724469832,440.94182659611),
 .UNSPECIFIED.);
#174=B_SPLINE_CURVE_WITH_KNOTS('',3,(#15729,#15730,#15731,#15732,#15733,
#15734,#15735,#15736,#15737,#15738),.UNSPECIFIED.,.F.,.F.,(4,1,1,1,1,1,
1,4),(440.94182659611,441.550707972031,442.54969147423,443.548674976429,
444.547658478629,445.546641980828,446.545625483027,447.225011903289),
 .UNSPECIFIED.);
#175=B_SPLINE_CURVE_WITH_KNOTS('',3,(#15740,#15741,#15742,#15743,#15744,
#15745,#15746,#15747,#15748,#15749),.UNSPECIFIED.,.F.,.F.,(4,1,1,1,1,1,
1,4),(447.225011903289,447.544608985226,448.543592487425,449.542575989624,
450.541559491824,451.540542994023,452.539526496222,453.50819303157),
 .UNSPECIFIED.);
#176=B_SPLINE_CURVE_WITH_KNOTS('',3,(#15751,#15752,#15753,#15754,#15755,
#15756,#15757,#15758,#15759,#15760,#15761,#15762,#15763,#15764,#15765,#15766,
#15767,#15768,#15769,#15770,#15771,#15772,#15773,#15774,#15775,#15776,#15777,
#15778,#15779,#15780,#15781,#15782,#15783,#15784,#15785,#15786,#15787,#15788,
#15789,#15790,#15791,#15792,#15793,#15794,#15795,#15796,#15797,#15798,#15799,
#15800,#15801,#15802,#15803,#15804,#15805,#15806,#15807,#15808,#15809,#15810,
#15811,#15812,#15813,#15814,#15815,#15816,#15817,#15818,#15819,#15820,#15821,
#15822,#15823,#15824,#15825,#15826,#15827,#15828,#15829,#15830,#15831,#15832,
#15833,#15834,#15835,#15836,#15837,#15838,#15839,#15840,#15841,#15842,#15843,
#15844,#15845,#15846,#15847,#15848,#15849,#15850,#15851,#15852,#15853,#15854,
#15855,#15856,#15857,#15858,#15859,#15860,#15861,#15862,#15863,#15864,#15865,
#15866,#15867,#15868,#15869,#15870,#15871,#15872,#15873,#15874,#15875,#15876,
#15877,#15878,#15879,#15880,#15881,#15882,#15883,#15884,#15885,#15886,#15887,
#15888,#15889,#15890,#15891,#15892,#15893,#15894,#15895,#15896,#15897,#15898,
#15899,#15900,#15901,#15902,#15903,#15904,#15905,#15906,#15907,#15908,#15909,
#15910,#15911,#15912,#15913,#15914,#15915,#15916,#15917,#15918,#15919,#15920,
#15921,#15922,#15923,#15924,#15925,#15926,#15927,#15928,#15929,#15930,#15931,
#15932,#15933,#15934,#15935,#15936,#15937,#15938,#15939,#15940,#15941,#15942,
#15943,#15944,#15945,#15946,#15947,#15948,#15949,#15950,#15951,#15952,#15953,
#15954,#15955,#15956,#15957,#15958,#15959,#15960,#15961,#15962,#15963,#15964,
#15965,#15966,#15967,#15968,#15969,#15970,#15971,#15972,#15973,#15974,#15975,
#15976,#15977,#15978,#15979,#15980,#15981,#15982,#15983,#15984,#15985,#15986,
#15987,#15988,#15989,#15990,#15991,#15992,#15993,#15994,#15995,#15996,#15997),
 .UNSPECIFIED.,.F.,.F.,(4,3,3,3,3,3,3,3,3,3,3,3,3,3,3,3,3,3,3,3,3,3,3,3,
3,3,3,3,3,3,3,3,3,3,3,3,3,3,3,3,3,3,3,3,3,3,3,3,3,3,3,3,3,3,3,3,3,3,3,3,
3,3,3,3,3,3,3,3,3,3,3,3,3,3,3,3,3,3,3,3,3,3,4),(453.508197210469,453.538509998421,
453.618474957208,453.698345545313,453.778139282339,453.85787362743,453.937565992737,
454.017245211278,454.096920975067,454.176609006935,454.256325034046,454.336128596977,
454.415981321654,454.495947731305,454.53749350062,454.617458459407,454.697329047512,
454.777122784539,454.85685712963,454.936549494937,455.016228713478,455.095904477267,
455.175592509135,455.255308536247,455.335112099177,455.414964823855,455.494931233505,
455.536477002819,455.616441961606,455.696312549711,455.776106286738,455.855840631829,
455.935532997136,456.015212215677,456.094887979466,456.174576011334,456.254292038446,
456.334095601376,456.413948326054,456.493914735704,456.535460505018,456.615425463805,
456.69529605191,456.775089788937,456.854824134028,456.934516499335,457.014195717876,
457.093871481666,457.173559513534,457.253275540645,457.333079103576,457.412931828254,
457.492898237904,457.534444007218,457.614408966005,457.69427955411,457.774073291137,
457.853807636228,457.933500001535,458.013179220076,458.092854983865,458.172543015733,
458.252259042845,458.332062605775,458.411915330453,458.491881740104,458.533427509417,
458.613392468204,458.693263056309,458.773056793335,458.852791138426,458.932483503733,
459.012162722274,459.091838486063,459.171526517931,459.251242545042,459.331046107972,
459.41089883265,459.4908652423,459.532411011616,459.635607913994,459.736866594815,
459.791382436132),.UNSPECIFIED.);
#177=B_SPLINE_CURVE_WITH_KNOTS('',3,(#15999,#16000,#16001,#16002,#16003,
#16004,#16005,#16006,#16007,#16008),.UNSPECIFIED.,.F.,.F.,(4,1,1,1,1,1,
1,4),(459.791382517649,460.531394513815,461.530378016014,462.529361518214,
463.528345020413,464.527328522612,465.526312024811,466.074567824828),
 .UNSPECIFIED.);
#178=B_SPLINE_CURVE_WITH_KNOTS('',3,(#16010,#16011,#16012,#16013,#16014,
#16015,#16016,#16017,#16018,#16019),.UNSPECIFIED.,.F.,.F.,(4,1,1,1,1,1,
1,4),(466.074567824828,466.52529552701,467.524279029209,468.523262531408,
469.522246033608,470.521229535807,471.520213038006,472.357753132008),
 .UNSPECIFIED.);
#179=B_SPLINE_CURVE_WITH_KNOTS('',3,(#16021,#16022,#16023,#16024,#16025,
#16026,#16027,#16028,#16029,#16030,#16031),.UNSPECIFIED.,.F.,.F.,(4,1,1,
1,1,1,1,1,4),(472.357753132008,472.519196540205,473.518180042404,474.517163544603,
475.516147046803,476.515130549002,477.514114051201,478.5130975534,478.640938439187),
 .UNSPECIFIED.);
#180=B_SPLINE_CURVE_WITH_KNOTS('',3,(#16033,#16034,#16035,#16036,#16037,
#16038,#16039,#16040,#16041,#16042,#16043,#16044,#16045,#16046,#16047,#16048,
#16049,#16050,#16051,#16052,#16053,#16054,#16055,#16056,#16057,#16058,#16059,
#16060,#16061,#16062,#16063,#16064,#16065,#16066,#16067,#16068,#16069,#16070,
#16071,#16072,#16073,#16074,#16075,#16076,#16077,#16078,#16079,#16080,#16081,
#16082,#16083,#16084,#16085,#16086,#16087,#16088,#16089,#16090,#16091,#16092,
#16093,#16094,#16095,#16096,#16097,#16098,#16099,#16100,#16101,#16102,#16103,
#16104,#16105,#16106,#16107,#16108,#16109,#16110,#16111,#16112,#16113,#16114,
#16115,#16116,#16117,#16118,#16119,#16120,#16121,#16122,#16123,#16124,#16125,
#16126,#16127,#16128,#16129,#16130,#16131,#16132,#16133,#16134,#16135,#16136,
#16137,#16138,#16139,#16140,#16141,#16142,#16143,#16144,#16145,#16146,#16147,
#16148,#16149,#16150,#16151,#16152,#16153,#16154,#16155,#16156,#16157,#16158,
#16159,#16160,#16161,#16162,#16163,#16164,#16165,#16166,#16167,#16168,#16169,
#16170,#16171,#16172,#16173,#16174,#16175,#16176,#16177,#16178,#16179,#16180,
#16181,#16182,#16183,#16184,#16185,#16186,#16187,#16188,#16189,#16190,#16191,
#16192,#16193,#16194,#16195,#16196,#16197,#16198,#16199,#16200,#16201,#16202,
#16203,#16204,#16205,#16206,#16207,#16208,#16209,#16210,#16211,#16212,#16213,
#16214,#16215,#16216,#16217,#16218,#16219,#16220,#16221,#16222,#16223,#16224,
#16225,#16226,#16227,#16228,#16229,#16230,#16231,#16232,#16233,#16234,#16235,
#16236,#16237,#16238,#16239,#16240,#16241,#16242,#16243,#16244,#16245,#16246,
#16247,#16248,#16249,#16250,#16251,#16252,#16253,#16254,#16255,#16256,#16257,
#16258,#16259,#16260,#16261,#16262,#16263,#16264,#16265,#16266,#16267,#16268,
#16269,#16270,#16271,#16272,#16273,#16274,#16275,#16276),.UNSPECIFIED.,
 .F.,.F.,(4,3,3,3,3,3,3,3,3,3,3,3,3,3,3,3,3,3,3,3,3,3,3,3,3,3,3,3,3,3,3,
3,3,3,3,3,3,3,3,3,3,3,3,3,3,3,3,3,3,3,3,3,3,3,3,3,3,3,3,3,3,3,3,3,3,3,3,
3,3,3,3,3,3,3,3,3,3,3,3,3,3,4),(478.640938439187,478.719706377143,478.798394573331,
478.877021407815,478.956403863788,479.034973428448,479.113540340611,479.19212112738,
479.272111109435,479.350808436616,479.431444746107,479.512081055599,479.592046014386,
479.671916602491,479.751710339518,479.831444684608,479.911137049915,479.990816268456,
480.070492032245,480.150180064113,480.229896091225,480.309699654155,480.389552378833,
480.469518788483,480.511064557798,480.591029516586,480.670900104691,480.750693841718,
480.830428186809,480.910120552116,480.989799770658,481.069475534447,481.149163566315,
481.228879593427,481.308683156358,481.388535881036,481.468502290686,481.510048059998,
481.590013018785,481.66988360689,481.749677343917,481.829411689009,481.909104054315,
481.988783272857,482.068459036646,482.148147068514,482.227863095625,482.307666658556,
482.387519383234,482.467485792884,482.509031562197,482.588996520984,482.668867109089,
482.748660846115,482.828395191206,482.908087556513,482.987766775054,483.067442538843,
483.147130570711,483.226846597823,483.306650160753,483.386502885431,483.466469295081,
483.508015064396,483.587980023183,483.667850611288,483.747644348314,483.827378693406,
483.907071058712,483.986750277253,484.066426041042,484.14611407291,484.225830100022,
484.305633662952,484.38548638763,484.465452797281,484.506998566595,484.594934491268,
484.682543461914,484.769947617553,484.857012922915,484.924123547619),
 .UNSPECIFIED.);
#181=B_SPLINE_CURVE_WITH_KNOTS('',3,(#16278,#16279,#16280,#16281,#16282,
#16283,#16284,#16285,#16286,#16287),.UNSPECIFIED.,.F.,.F.,(4,1,1,1,1,1,
1,4),(484.924123746367,485.505982068794,486.504965570993,487.503949073193,
488.502932575392,489.501916077591,490.50089957979,491.207309053546),
 .UNSPECIFIED.);
#182=B_SPLINE_CURVE_WITH_KNOTS('',3,(#16289,#16290,#16291,#16292,#16293,
#16294,#16295,#16296,#16297,#16298,#16299,#16300,#16301,#16302,#16303,#16304,
#16305,#16306,#16307,#16308,#16309,#16310,#16311,#16312,#16313,#16314,#16315,
#16316,#16317,#16318,#16319,#16320,#16321,#16322,#16323,#16324,#16325,#16326,
#16327,#16328,#16329,#16330,#16331,#16332,#16333,#16334,#16335,#16336,#16337,
#16338,#16339,#16340,#16341,#16342,#16343,#16344,#16345,#16346,#16347,#16348,
#16349,#16350,#16351,#16352,#16353,#16354,#16355,#16356,#16357,#16358,#16359,
#16360,#16361,#16362,#16363,#16364,#16365,#16366,#16367,#16368,#16369,#16370,
#16371,#16372,#16373,#16374,#16375,#16376,#16377,#16378,#16379,#16380,#16381,
#16382,#16383,#16384,#16385,#16386,#16387,#16388,#16389,#16390,#16391,#16392,
#16393,#16394,#16395,#16396,#16397,#16398,#16399,#16400,#16401,#16402,#16403,
#16404,#16405,#16406,#16407,#16408,#16409,#16410,#16411,#16412,#16413,#16414,
#16415,#16416,#16417,#16418,#16419,#16420,#16421,#16422,#16423,#16424,#16425,
#16426,#16427,#16428,#16429,#16430,#16431,#16432,#16433,#16434,#16435,#16436,
#16437,#16438,#16439,#16440,#16441,#16442,#16443,#16444,#16445,#16446,#16447,
#16448,#16449,#16450,#16451,#16452,#16453,#16454,#16455,#16456,#16457,#16458,
#16459,#16460,#16461,#16462,#16463,#16464,#16465,#16466,#16467,#16468,#16469,
#16470,#16471,#16472,#16473,#16474,#16475,#16476,#16477,#16478,#16479,#16480,
#16481,#16482,#16483,#16484,#16485,#16486,#16487,#16488,#16489,#16490,#16491,
#16492,#16493,#16494,#16495,#16496,#16497,#16498,#16499,#16500,#16501,#16502,
#16503,#16504,#16505,#16506,#16507,#16508,#16509,#16510,#16511,#16512,#16513,
#16514,#16515,#16516,#16517,#16518,#16519,#16520,#16521,#16522,#16523,#16524,
#16525,#16526,#16527,#16528,#16529,#16530,#16531,#16532),.UNSPECIFIED.,
 .F.,.F.,(4,3,3,3,3,3,3,3,3,3,3,3,3,3,3,3,3,3,3,3,3,3,3,3,3,3,3,3,3,3,3,
3,3,3,3,3,3,3,3,3,3,3,3,3,3,3,3,3,3,3,3,3,3,3,3,3,3,3,3,3,3,3,3,3,3,3,3,
3,3,3,3,3,3,3,3,3,3,3,3,3,3,4),(491.207309221467,491.304080701035,491.402189558315,
491.499883081989,491.579848040776,491.65971862888,491.739512365907,491.819246710998,
491.898939076304,491.978618294845,492.058294058634,492.137982090501,492.217698117612,
492.297501680543,492.37735440522,492.45732081487,492.498866584188,492.578831542976,
492.65870213108,492.738495868107,492.818230213199,492.897922578506,492.977601797047,
493.057277560837,493.136965592705,493.216681619817,493.296485182747,493.376337907425,
493.456304317076,493.497850086388,493.577815045175,493.65768563328,493.737479370307,
493.817213715398,493.896906080705,493.976585299246,494.056261063035,494.135949094903,
494.215665122015,494.295468684945,494.375321409623,494.455287819274,494.496833588587,
494.576798547374,494.656669135479,494.736462872505,494.816197217596,494.895889582903,
494.975568801444,495.055244565233,495.134932597101,495.214648624212,495.294452187142,
495.37430491182,495.454271321471,495.495817090786,495.575782049573,495.655652637678,
495.735446374705,495.815180719796,495.894873085103,495.974552303644,496.054228067433,
496.133916099301,496.213632126412,496.293435689343,496.373288414021,496.453254823671,
496.494800592985,496.57471819498,496.654541447734,496.734287917752,496.81397511075,
496.89362048528,496.973252939931,497.052882172046,497.132523946332,497.212194032043,
497.291951648498,497.37175879078,497.451678816343,497.490494360726),
 .UNSPECIFIED.);
#183=B_SPLINE_CURVE_WITH_KNOTS('',3,(#16534,#16535,#16536,#16537,#16538,
#16539,#16540,#16541,#16542,#16543,#16544,#16545),.UNSPECIFIED.,.F.,.F.,
(4,2,1,1,1,1,1,1,4),(497.490494360726,497.493784095184,498.492767597383,
499.491751099583,500.490734601782,501.489718103981,502.48870160618,503.487685108379,
503.773679667906),.UNSPECIFIED.);
#184=B_SPLINE_CURVE_WITH_KNOTS('',3,(#16547,#16548,#16549,#16550,#16551,
#16552,#16553,#16554,#16555,#16556),.UNSPECIFIED.,.F.,.F.,(4,1,1,1,1,1,
1,4),(503.773679667906,504.486668610578,505.485652112778,506.484635614977,
507.483619117176,508.482602619375,509.481586121574,510.056864975085),
 .UNSPECIFIED.);
#185=B_SPLINE_CURVE_WITH_KNOTS('',3,(#16558,#16559,#16560,#16561,#16562,
#16563,#16564,#16565,#16566,#16567),.UNSPECIFIED.,.F.,.F.,(4,1,1,1,1,1,
1,4),(510.056864975085,510.480569623773,511.479553125973,512.478536628172,
513.477520130371,514.47650363257,515.475487134769,516.340050282265),
 .UNSPECIFIED.);
#186=B_SPLINE_CURVE_WITH_KNOTS('',3,(#16569,#16570,#16571,#16572,#16573,
#16574,#16575,#16576,#16577,#16578,#16579),.UNSPECIFIED.,.F.,.F.,(4,1,1,
1,1,1,1,1,4),(516.340050282265,516.474470636968,517.473454139167,518.472437641367,
519.471421143566,520.470404645765,521.469388147964,522.468371650163,522.623235589444),
 .UNSPECIFIED.);
#187=B_SPLINE_CURVE_WITH_KNOTS('',3,(#16581,#16582,#16583,#16584,#16585,
#16586,#16587,#16588,#16589,#16590),.UNSPECIFIED.,.F.,.F.,(4,1,1,1,1,1,
1,4),(522.623235589444,523.467355152363,524.466338654562,525.465322156761,
526.46430565896,527.463289161159,528.462272663358,528.906420896624),
 .UNSPECIFIED.);
#188=B_SPLINE_CURVE_WITH_KNOTS('',3,(#16592,#16593,#16594,#16595,#16596,
#16597,#16598,#16599,#16600,#16601),.UNSPECIFIED.,.F.,.F.,(4,1,1,1,1,1,
1,4),(528.906420896624,529.461256165558,530.460239667757,531.459223169956,
532.458206672155,533.457190174354,534.456173676553,535.189606203803),
 .UNSPECIFIED.);
#189=B_SPLINE_CURVE_WITH_KNOTS('',3,(#16603,#16604,#16605,#16606,#16607,
#16608,#16609,#16610,#16611,#16612,#16613),.UNSPECIFIED.,.F.,.F.,(4,1,1,
1,1,1,1,1,4),(535.189606203803,535.455157178753,536.454140680952,537.453124183151,
538.45210768535,539.451091187549,540.450074689748,541.449058191948,541.472791510983),
 .UNSPECIFIED.);
#190=B_SPLINE_CURVE_WITH_KNOTS('',3,(#16615,#16616,#16617,#16618,#16619,
#16620,#16621,#16622,#16623,#16624,#16625,#16626,#16627,#16628,#16629,#16630,
#16631,#16632,#16633,#16634,#16635,#16636,#16637,#16638,#16639,#16640,#16641,
#16642,#16643,#16644,#16645,#16646,#16647,#16648,#16649,#16650,#16651,#16652,
#16653,#16654,#16655,#16656,#16657,#16658,#16659,#16660,#16661,#16662,#16663,
#16664,#16665,#16666,#16667,#16668,#16669,#16670,#16671,#16672,#16673,#16674,
#16675,#16676,#16677,#16678,#16679,#16680,#16681,#16682,#16683,#16684,#16685,
#16686,#16687,#16688,#16689,#16690,#16691,#16692,#16693,#16694,#16695,#16696,
#16697,#16698,#16699,#16700,#16701,#16702,#16703,#16704,#16705,#16706,#16707,
#16708,#16709,#16710,#16711,#16712,#16713,#16714,#16715,#16716,#16717,#16718,
#16719,#16720,#16721,#16722,#16723,#16724,#16725,#16726,#16727,#16728,#16729,
#16730,#16731,#16732,#16733,#16734,#16735,#16736,#16737,#16738,#16739,#16740,
#16741,#16742,#16743,#16744,#16745,#16746,#16747,#16748,#16749,#16750,#16751,
#16752,#16753,#16754,#16755,#16756,#16757,#16758,#16759,#16760,#16761,#16762,
#16763,#16764,#16765,#16766,#16767,#16768,#16769,#16770,#16771,#16772,#16773,
#16774,#16775,#16776,#16777,#16778,#16779,#16780,#16781,#16782,#16783,#16784,
#16785,#16786,#16787,#16788,#16789,#16790,#16791,#16792,#16793,#16794,#16795,
#16796,#16797,#16798,#16799,#16800,#16801,#16802,#16803,#16804,#16805,#16806,
#16807,#16808,#16809,#16810,#16811,#16812,#16813,#16814,#16815,#16816,#16817,
#16818,#16819,#16820,#16821,#16822,#16823,#16824,#16825,#16826,#16827,#16828,
#16829,#16830,#16831,#16832,#16833,#16834,#16835,#16836,#16837,#16838,#16839,
#16840,#16841,#16842,#16843,#16844,#16845,#16846,#16847,#16848,#16849,#16850,
#16851,#16852,#16853,#16854,#16855,#16856,#16857,#16858,#16859,#16860,#16861),
 .UNSPECIFIED.,.F.,.F.,(4,3,3,3,3,3,3,3,3,3,3,3,3,3,3,3,3,3,3,3,3,3,3,3,
3,3,3,3,3,3,3,3,3,3,3,3,3,3,3,3,3,3,3,3,3,3,3,3,3,3,3,3,3,3,3,3,3,3,3,3,
3,3,3,3,3,3,3,3,3,3,3,3,3,3,3,3,3,3,3,3,3,3,4),(541.472791510983,541.552434384195,
541.631983655514,541.711457142406,541.790872599625,541.87301873644,541.952382639305,
542.031745690708,542.111123880599,542.190533205499,542.270030489991,542.349580264739,
542.42923733723,542.448041694147,542.528006652934,542.607877241039,542.687670978065,
542.767405323156,542.847097688464,542.926776907005,543.006452670794,543.086140702662,
543.165856729773,543.245660292703,543.325513017381,543.405479427032,543.447025196346,
543.526990155133,543.606860743238,543.686654480265,543.766388825356,543.846081190663,
543.925760409204,544.005436172993,544.085124204861,544.164840231972,544.244643794903,
544.32449651958,544.404462929231,544.446008698545,544.525973657332,544.605844245437,
544.685637982464,544.765372327555,544.845064692863,544.924743911404,545.004419675193,
545.084107707061,545.163823734172,545.243627297103,545.32348002178,545.403446431431,
545.444992200744,545.524957159531,545.604827747636,545.684621484663,545.764355829754,
545.844048195061,545.923727413602,546.003403177391,546.083091209259,546.16280723637,
546.242610799301,546.322463523979,546.402429933629,546.443975702943,546.52394066173,
546.603811249835,546.683604986862,546.763339331953,546.84303169726,546.922710915801,
547.00238667959,547.082074711458,547.161790738569,547.2415943015,547.321447026177,
547.401413435828,547.442959205142,547.53892448688,547.634366343838,547.72884563209,
547.755976610976),.UNSPECIFIED.);
#191=B_SPLINE_CURVE_WITH_KNOTS('',3,(#16863,#16864,#16865,#16866,#16867,
#16868,#16869,#16870,#16871,#16872),.UNSPECIFIED.,.F.,.F.,(4,1,1,1,1,1,
1,4),(547.755976818162,548.441942707342,549.440926209541,550.43990971174,
551.438893213939,552.437876716138,553.436860218338,554.039162125342),
 .UNSPECIFIED.);
#192=B_SPLINE_CURVE_WITH_KNOTS('',3,(#16874,#16875,#16876,#16877,#16878,
#16879,#16880,#16881,#16882,#16883),.UNSPECIFIED.,.F.,.F.,(4,1,1,1,1,1,
1,4),(554.039162125342,554.435843720537,555.434827222736,556.433810724935,
557.432794227134,558.431777729333,559.430761231533,560.322347432522),
 .UNSPECIFIED.);
#193=B_SPLINE_CURVE_WITH_KNOTS('',3,(#16885,#16886,#16887,#16888,#16889,
#16890,#16891,#16892,#16893,#16894,#16895),.UNSPECIFIED.,.F.,.F.,(4,1,1,
1,1,1,1,1,4),(560.322347432522,560.429744733732,561.428728235931,562.42771173813,
563.426695240329,564.425678742528,565.424662244728,566.423645746927,566.605532739701),
 .UNSPECIFIED.);
#194=B_SPLINE_CURVE_WITH_KNOTS('',3,(#16897,#16898,#16899,#16900,#16901,
#16902,#16903,#16904,#16905,#16906),.UNSPECIFIED.,.F.,.F.,(4,1,1,1,1,1,
1,4),(566.605532739701,567.422629249126,568.421612751325,569.420596253524,
570.419579755723,571.418563257923,572.417546760122,572.888718046881),
 .UNSPECIFIED.);
#195=B_SPLINE_CURVE_WITH_KNOTS('',3,(#16908,#16909,#16910,#16911,#16912,
#16913,#16914,#16915,#16916,#16917),.UNSPECIFIED.,.F.,.F.,(4,1,1,1,1,1,
1,4),(572.888718046881,573.416530262321,574.41551376452,575.414497266719,
576.413480768918,577.412464271117,578.411447773317,579.17190335406),
 .UNSPECIFIED.);
#196=B_SPLINE_CURVE_WITH_KNOTS('',3,(#16919,#16920,#16921,#16922,#16923,
#16924,#16925,#16926,#16927,#16928,#16929),.UNSPECIFIED.,.F.,.F.,(4,1,1,
1,1,1,1,1,4),(579.17190335406,579.410431275516,580.409414777715,581.408398279914,
582.407381782113,583.406365284312,584.405348786512,585.404332288711,585.45508866124),
 .UNSPECIFIED.);
#197=B_SPLINE_CURVE_WITH_KNOTS('',3,(#16931,#16932,#16933,#16934,#16935,
#16936,#16937,#16938,#16939,#16940),.UNSPECIFIED.,.F.,.F.,(4,1,1,1,1,1,
1,4),(585.45508866124,586.40331579091,587.402299293109,588.401282795308,
589.400266297508,590.399249799707,591.398233301906,591.738266415292),
 .UNSPECIFIED.);
#198=B_SPLINE_CURVE_WITH_KNOTS('',3,(#16942,#16943,#16944,#16945,#16946,
#16947,#16948,#16949,#16950,#16951,#16952,#16953,#16954,#16955,#16956,#16957,
#16958,#16959,#16960,#16961,#16962,#16963,#16964,#16965,#16966,#16967,#16968,
#16969,#16970,#16971,#16972,#16973,#16974,#16975,#16976,#16977,#16978,#16979,
#16980,#16981,#16982,#16983,#16984,#16985,#16986,#16987,#16988,#16989,#16990,
#16991,#16992,#16993,#16994,#16995,#16996,#16997,#16998,#16999,#17000,#17001,
#17002,#17003,#17004,#17005,#17006,#17007,#17008,#17009,#17010,#17011,#17012,
#17013,#17014,#17015,#17016,#17017,#17018,#17019,#17020,#17021,#17022,#17023,
#17024,#17025,#17026,#17027,#17028,#17029,#17030,#17031,#17032,#17033,#17034,
#17035,#17036,#17037,#17038,#17039,#17040,#17041,#17042,#17043,#17044,#17045,
#17046,#17047,#17048,#17049,#17050,#17051,#17052,#17053,#17054,#17055,#17056,
#17057,#17058,#17059,#17060,#17061,#17062,#17063,#17064,#17065,#17066,#17067,
#17068,#17069,#17070,#17071,#17072,#17073,#17074,#17075,#17076,#17077,#17078,
#17079,#17080,#17081,#17082,#17083,#17084,#17085,#17086,#17087,#17088,#17089,
#17090,#17091,#17092,#17093,#17094,#17095,#17096,#17097,#17098,#17099,#17100,
#17101,#17102,#17103,#17104,#17105,#17106,#17107,#17108,#17109,#17110,#17111,
#17112,#17113,#17114,#17115,#17116,#17117,#17118,#17119,#17120,#17121,#17122,
#17123,#17124,#17125,#17126,#17127,#17128,#17129,#17130,#17131,#17132,#17133,
#17134,#17135,#17136,#17137,#17138,#17139,#17140,#17141,#17142,#17143,#17144,
#17145,#17146,#17147,#17148,#17149,#17150,#17151,#17152,#17153,#17154,#17155,
#17156,#17157,#17158,#17159,#17160,#17161,#17162,#17163,#17164,#17165,#17166,
#17167,#17168,#17169,#17170,#17171,#17172,#17173,#17174,#17175,#17176,#17177,
#17178,#17179,#17180,#17181,#17182,#17183,#17184,#17185,#17186,#17187,#17188),
 .UNSPECIFIED.,.F.,.F.,(4,3,3,3,3,3,3,3,3,3,3,3,3,3,3,3,3,3,3,3,3,3,3,3,
3,3,3,3,3,3,3,3,3,3,3,3,3,3,3,3,3,3,3,3,3,3,3,3,3,3,3,3,3,3,3,3,3,3,3,3,
3,3,3,3,3,3,3,3,3,3,3,3,3,3,3,3,3,3,3,3,3,3,4),(591.738273968419,591.82064182288,
591.90035776133,591.980080161589,592.059824638625,592.139606817585,592.219485387332,
592.299421470385,592.379470642451,592.397216804105,592.477181762892,592.557052350997,
592.636846088023,592.716580433114,592.796272798421,592.875952016962,592.955627780751,
593.035315812619,593.11503183973,593.194835402661,593.274688127339,593.354654536989,
593.396200306304,593.476165265091,593.556035853196,593.635829590223,593.715563935314,
593.795256300621,593.874935519162,593.954611282952,594.034299314819,594.114015341931,
594.193818904861,594.273671629539,594.35363803919,594.395183808503,594.47514876729,
594.555019355395,594.634813092421,594.714547437512,594.79423980282,594.873919021361,
594.95359478515,595.033282817018,595.112998844129,595.19280240706,595.272655131737,
595.352621541388,595.394167310702,595.474132269489,595.554002857594,595.633796594621,
595.713530939713,595.793223305019,595.872902523561,595.95257828735,596.032266319218,
596.11198234633,596.191785909261,596.271638633939,596.35160504359,596.393150812902,
596.473115771689,596.552986359794,596.632780096821,596.712514441912,596.792206807219,
596.871886025761,596.95156178955,597.031249821418,597.110965848529,597.19076941146,
597.270622136138,597.350588545789,597.392134315101,597.472660730037,597.553090017382,
597.633437415374,597.713718108436,597.793943515459,597.874135612635,597.954320611889,
598.021459275599),.UNSPECIFIED.);
#199=B_SPLINE_CURVE_WITH_KNOTS('',3,(#17190,#17191,#17192,#17193,#17194,
#17195,#17196,#17197,#17198,#17199),.UNSPECIFIED.,.F.,.F.,(4,1,1,1,1,1,
1,4),(598.021466925895,598.3911178173,599.390101319499,600.389084821698,
601.388068323897,602.387051826097,603.386035328296,604.304644582779),
 .UNSPECIFIED.);
#200=B_SPLINE_CURVE_WITH_KNOTS('',3,(#17201,#17202,#17203,#17204,#17205,
#17206,#17207,#17208,#17209,#17210,#17211,#17212),.UNSPECIFIED.,.F.,.F.,
(4,2,1,1,1,1,1,1,4),(604.304644582779,604.385018830495,605.384002332694,
606.382985834893,607.381969337092,608.380952839292,609.379936341491,610.37891984369,
610.587829889958),.UNSPECIFIED.);
#201=B_SPLINE_CURVE_WITH_KNOTS('',3,(#17214,#17215,#17216,#17217,#17218,
#17219,#17220,#17221,#17222,#17223),.UNSPECIFIED.,.F.,.F.,(4,1,1,1,1,1,
1,4),(610.587829889958,611.377903345889,612.376886848088,613.375870350287,
614.374853852486,615.373837354686,616.372820856885,616.871015197138),
 .UNSPECIFIED.);
#202=B_SPLINE_CURVE_WITH_KNOTS('',3,(#17225,#17226,#17227,#17228,#17229,
#17230,#17231,#17232,#17233,#17234),.UNSPECIFIED.,.F.,.F.,(4,1,1,1,1,1,
1,4),(616.871015197138,617.371804359084,618.370787861283,619.369771363482,
620.368754865682,621.367738367881,622.36672187008,623.154200504317),
 .UNSPECIFIED.);
#203=B_SPLINE_CURVE_WITH_KNOTS('',3,(#17236,#17237,#17238,#17239,#17240,
#17241,#17242,#17243,#17244,#17245,#17246),.UNSPECIFIED.,.F.,.F.,(4,1,1,
1,1,1,1,1,4),(623.154200504317,623.365705372279,624.364688874478,625.363672376677,
626.362655878877,627.361639381076,628.360622883275,629.359606385474,629.437385811497),
 .UNSPECIFIED.);
#204=B_SPLINE_CURVE_WITH_KNOTS('',3,(#17248,#17249,#17250,#17251,#17252,
#17253,#17254,#17255,#17256,#17257),.UNSPECIFIED.,.F.,.F.,(4,1,1,1,1,1,
1,4),(629.437385811497,630.358589887673,631.357573389873,632.356556892072,
633.355540394271,634.35452389647,635.353507398669,635.72056345413),
 .UNSPECIFIED.);
#205=B_SPLINE_CURVE_WITH_KNOTS('',3,(#17259,#17260,#17261,#17262,#17263,
#17264,#17265,#17266,#17267,#17268,#17269,#17270,#17271,#17272,#17273,#17274,
#17275,#17276,#17277,#17278,#17279,#17280,#17281,#17282,#17283,#17284,#17285,
#17286,#17287,#17288,#17289,#17290,#17291,#17292,#17293,#17294,#17295,#17296,
#17297,#17298,#17299,#17300,#17301,#17302,#17303,#17304,#17305,#17306,#17307,
#17308,#17309,#17310,#17311,#17312,#17313,#17314,#17315,#17316,#17317,#17318,
#17319,#17320,#17321,#17322,#17323,#17324,#17325,#17326,#17327,#17328,#17329,
#17330,#17331,#17332,#17333,#17334,#17335,#17336,#17337,#17338,#17339,#17340,
#17341,#17342,#17343,#17344,#17345,#17346,#17347,#17348,#17349,#17350,#17351,
#17352,#17353,#17354,#17355,#17356,#17357,#17358,#17359,#17360,#17361,#17362,
#17363,#17364,#17365,#17366,#17367,#17368,#17369,#17370,#17371,#17372,#17373,
#17374,#17375,#17376,#17377,#17378,#17379,#17380,#17381,#17382,#17383,#17384,
#17385,#17386,#17387,#17388,#17389,#17390,#17391,#17392,#17393,#17394,#17395,
#17396,#17397,#17398,#17399,#17400,#17401,#17402,#17403,#17404,#17405,#17406,
#17407,#17408,#17409,#17410,#17411,#17412,#17413,#17414,#17415,#17416,#17417,
#17418,#17419,#17420,#17421,#17422,#17423,#17424,#17425,#17426,#17427,#17428,
#17429,#17430,#17431,#17432,#17433,#17434,#17435,#17436,#17437,#17438,#17439,
#17440,#17441,#17442,#17443,#17444,#17445,#17446,#17447,#17448,#17449,#17450,
#17451,#17452,#17453,#17454,#17455,#17456,#17457,#17458,#17459,#17460,#17461,
#17462,#17463,#17464,#17465,#17466,#17467,#17468,#17469,#17470,#17471,#17472,
#17473,#17474,#17475,#17476,#17477,#17478,#17479,#17480,#17481,#17482,#17483,
#17484,#17485,#17486,#17487,#17488,#17489,#17490,#17491,#17492,#17493,#17494,
#17495,#17496,#17497,#17498,#17499,#17500,#17501,#17502,#17503,#17504,#17505),
 .UNSPECIFIED.,.F.,.F.,(4,3,3,3,3,3,3,3,3,3,3,3,3,3,3,3,3,3,3,3,3,3,3,3,
3,3,3,3,3,3,3,3,3,3,3,3,3,3,3,3,3,3,3,3,3,3,3,3,3,3,3,3,3,3,3,3,3,3,3,3,
3,3,3,3,3,3,3,3,3,3,3,3,3,3,3,3,3,3,3,3,3,3,4),(635.720571118676,635.800716360848,
635.880864171963,635.961029670184,636.041227981188,636.121525941313,636.201875952468,
636.282358567307,636.352490900868,636.432453727681,636.512322182468,636.592113786839,
636.671846001927,636.751536241864,636.831213348658,636.910887009352,636.990572948562,
637.070286895249,637.15008840676,637.229939093392,637.309903503355,637.351474403067,
637.431440742958,637.511312700702,637.591107794774,637.670843483185,637.750537176951,
637.830217697708,637.909894747326,637.989584047587,638.069301324594,638.149106103173,
638.228960025913,638.308927596002,638.350457905267,638.430427643991,638.510303040276,
638.590101608879,638.669840804149,638.749538033481,638.829222121093,638.908902756573,
638.988595658521,639.068316549863,639.148124943528,639.227982487151,639.307953655806,
639.349441407466,639.429391681465,639.509247568071,639.58902660077,639.668746252476,
639.748423949045,639.828088581936,639.907749812979,639.987423377342,640.067125014586,
640.146914377732,640.22675298909,640.306705541614,640.348424909665,640.428402857143,
640.508286367581,640.588092949365,640.66784005044,640.747545071756,640.82723675789,
640.906924871261,640.986625124445,641.066353234259,641.146168609493,641.226033010865,
641.306010786103,641.347408411864,641.429451913613,641.509413080617,641.589297472675,
641.669120771521,641.752779685104,641.832531129424,641.912269375975,641.992019605056,
642.003756425856),.UNSPECIFIED.);
#206=B_SPLINE_CURVE_WITH_KNOTS('',3,(#17507,#17508,#17509,#17510,#17511,
#17512,#17513,#17514),.UNSPECIFIED.,.F.,.F.,(4,1,1,1,1,4),(642.003763862697,
642.346391914063,643.345375416262,644.344358918462,645.343342420661,646.269689253992),
 .UNSPECIFIED.);
#207=B_SPLINE_CURVE_WITH_KNOTS('',3,(#17518,#17519,#17520,#17521,#17522,
#17523,#17524,#17525),.UNSPECIFIED.,.F.,.F.,(4,1,1,1,1,4),(-648.340292927258,
-647.840801176158,-647.341309425059,-646.342325922859,-645.34334242066,
-644.977443081154),.UNSPECIFIED.);
#208=B_SPLINE_CURVE_WITH_KNOTS('',3,(#17527,#17528,#17529,#17530,#17531,
#17532,#17533,#17534,#17535,#17536),.UNSPECIFIED.,.F.,.F.,(4,1,1,1,1,1,
1,4),(-644.977443081154,-644.344358918461,-643.345375416262,-642.346391914063,
-641.347408411864,-640.348424909664,-639.349441407465,-638.694257773975),
 .UNSPECIFIED.);
#209=B_SPLINE_CURVE_WITH_KNOTS('',3,(#17538,#17539,#17540,#17541,#17542,
#17543,#17544,#17545,#17546,#17547,#17548,#17549,#17550,#17551,#17552,#17553,
#17554,#17555,#17556,#17557,#17558,#17559,#17560,#17561,#17562,#17563,#17564,
#17565,#17566,#17567,#17568,#17569,#17570,#17571,#17572,#17573,#17574,#17575,
#17576,#17577,#17578,#17579,#17580,#17581,#17582,#17583,#17584,#17585,#17586,
#17587,#17588,#17589,#17590,#17591,#17592,#17593,#17594,#17595,#17596,#17597,
#17598,#17599,#17600,#17601,#17602,#17603,#17604,#17605,#17606,#17607,#17608,
#17609,#17610,#17611,#17612,#17613,#17614,#17615,#17616,#17617,#17618,#17619,
#17620,#17621,#17622,#17623,#17624,#17625,#17626,#17627,#17628,#17629,#17630,
#17631,#17632,#17633,#17634,#17635,#17636,#17637,#17638,#17639,#17640,#17641,
#17642,#17643,#17644,#17645,#17646,#17647,#17648,#17649,#17650,#17651,#17652,
#17653,#17654,#17655,#17656,#17657,#17658,#17659,#17660,#17661,#17662,#17663,
#17664,#17665,#17666,#17667,#17668,#17669,#17670,#17671,#17672,#17673,#17674,
#17675,#17676,#17677,#17678,#17679,#17680,#17681,#17682,#17683,#17684,#17685,
#17686,#17687,#17688,#17689,#17690,#17691,#17692,#17693,#17694,#17695,#17696,
#17697,#17698,#17699,#17700,#17701,#17702,#17703,#17704,#17705,#17706,#17707,
#17708,#17709,#17710,#17711,#17712,#17713,#17714,#17715,#17716,#17717,#17718,
#17719,#17720,#17721,#17722,#17723,#17724,#17725,#17726,#17727,#17728,#17729,
#17730,#17731,#17732,#17733,#17734,#17735,#17736,#17737,#17738,#17739,#17740,
#17741,#17742,#17743,#17744,#17745,#17746,#17747,#17748,#17749,#17750,#17751,
#17752,#17753,#17754,#17755,#17756,#17757,#17758,#17759,#17760,#17761,#17762,
#17763,#17764,#17765,#17766,#17767,#17768,#17769,#17770,#17771,#17772,#17773,
#17774,#17775,#17776,#17777,#17778,#17779,#17780,#17781),.UNSPECIFIED.,
 .F.,.F.,(4,3,3,3,3,3,3,3,3,3,3,3,3,3,3,3,3,3,3,3,3,3,3,3,3,3,3,3,3,3,3,
3,3,3,3,3,3,3,3,3,3,3,3,3,3,3,3,3,3,3,3,3,3,3,3,3,3,3,3,3,3,3,3,3,3,3,3,
3,3,3,3,3,3,3,3,3,3,3,3,3,3,4),(-638.694257653504,-638.602314147676,-638.509906521229,
-638.416901408164,-638.350457905266,-638.270491791684,-638.190620021241,
-638.110825075614,-638.031089496909,-637.951395874201,-637.871715366522,
-637.792038293996,-637.712348934841,-637.632631562926,-637.552826635138,
-637.472972532192,-637.393004735029,-637.351474403067,-637.27151143441,
-637.191642862227,-637.111851164813,-637.032118880961,-636.952428596482,
-636.872751481486,-636.793077835144,-636.713391932841,-636.633678045632,
-636.553876627634,-636.474026053943,-636.394061786297,-636.352490900868,
-636.272525125158,-636.192653713066,-636.112859145831,-636.033123965146,
-635.953430759684,-635.873750696862,-635.794074086318,-635.714385205951,
-635.634668329325,-635.554863919623,-635.475010348465,-635.395043100077,
-635.353507398669,-635.27354234991,-635.193671668647,-635.113877835379,
-635.034143391066,-634.954450923656,-634.874771599002,-634.795095726619,
-634.715407583757,-634.635691443333,-634.555887764108,-634.476034921271,
-634.396068391543,-634.354523896469,-634.274559218377,-634.194688914776,
-634.114895465763,-634.035161411905,-633.955469340762,-633.87579041984,
-633.796114955786,-633.716427225518,-633.63671150162,-633.556908242843,
-633.477055823306,-633.397089717725,-633.35554039427,-633.276230505782,
-633.197014541243,-633.117874400493,-633.038792051091,-632.959743562529,
-632.880711844586,-632.801680658467,-632.722633768204,-632.643509498184,
-632.564346038251,-632.485064970735,-632.411072466795),.UNSPECIFIED.);
#210=B_SPLINE_CURVE_WITH_KNOTS('',3,(#17783,#17784,#17785,#17786,#17787,
#17788,#17789,#17790,#17791,#17792,#17793,#17794),.UNSPECIFIED.,.F.,.F.,
(4,2,1,1,1,1,1,1,4),(-632.411072466795,-632.356556892071,-631.357573389872,
-630.358589887673,-629.359606385474,-628.360622883274,-627.361639381075,
-626.362655878876,-626.127887159616),.UNSPECIFIED.);
#211=B_SPLINE_CURVE_WITH_KNOTS('',3,(#17796,#17797,#17798,#17799,#17800,
#17801,#17802,#17803,#17804,#17805),.UNSPECIFIED.,.F.,.F.,(4,1,1,1,1,1,
1,4),(-626.127887159616,-625.363672376677,-624.364688874478,-623.365705372279,
-622.366721870079,-621.36773836788,-620.368754865681,-619.844701852436),
 .UNSPECIFIED.);
#212=B_SPLINE_CURVE_WITH_KNOTS('',3,(#17807,#17808,#17809,#17810,#17811,
#17812,#17813,#17814,#17815,#17816),.UNSPECIFIED.,.F.,.F.,(4,1,1,1,1,1,
1,4),(-619.844701852436,-619.369771363482,-618.370787861283,-617.371804359084,
-616.372820856884,-615.373837354685,-614.374853852486,-613.561521139307),
 .UNSPECIFIED.);
#213=B_SPLINE_CURVE_WITH_KNOTS('',3,(#17818,#17819,#17820,#17821,#17822,
#17823,#17824,#17825,#17826,#17827,#17828,#17829,#17830,#17831,#17832,#17833,
#17834,#17835,#17836,#17837,#17838,#17839,#17840,#17841,#17842,#17843,#17844,
#17845,#17846,#17847,#17848,#17849,#17850,#17851,#17852,#17853,#17854,#17855,
#17856,#17857,#17858,#17859,#17860,#17861,#17862,#17863,#17864,#17865,#17866,
#17867,#17868,#17869,#17870,#17871,#17872,#17873,#17874,#17875,#17876,#17877,
#17878,#17879,#17880,#17881,#17882,#17883,#17884,#17885,#17886,#17887,#17888,
#17889,#17890,#17891,#17892,#17893,#17894,#17895,#17896,#17897,#17898,#17899,
#17900,#17901,#17902,#17903,#17904,#17905,#17906,#17907,#17908,#17909,#17910,
#17911,#17912,#17913,#17914,#17915,#17916,#17917,#17918,#17919,#17920,#17921,
#17922,#17923,#17924,#17925,#17926,#17927,#17928,#17929,#17930,#17931,#17932,
#17933,#17934,#17935,#17936,#17937,#17938,#17939,#17940,#17941,#17942,#17943,
#17944,#17945,#17946,#17947,#17948,#17949,#17950,#17951,#17952,#17953,#17954,
#17955,#17956,#17957,#17958,#17959,#17960,#17961,#17962,#17963,#17964,#17965,
#17966,#17967,#17968,#17969,#17970,#17971,#17972,#17973,#17974,#17975,#17976,
#17977,#17978,#17979,#17980,#17981,#17982,#17983,#17984,#17985,#17986,#17987,
#17988,#17989,#17990,#17991,#17992,#17993,#17994,#17995,#17996,#17997,#17998,
#17999,#18000,#18001,#18002,#18003,#18004,#18005,#18006,#18007,#18008,#18009,
#18010,#18011,#18012,#18013,#18014,#18015,#18016,#18017,#18018,#18019,#18020,
#18021,#18022,#18023,#18024,#18025,#18026,#18027,#18028,#18029,#18030,#18031,
#18032,#18033,#18034,#18035,#18036,#18037,#18038,#18039,#18040,#18041,#18042,
#18043,#18044,#18045,#18046,#18047,#18048,#18049,#18050,#18051,#18052,#18053,
#18054,#18055,#18056,#18057,#18058,#18059,#18060,#18061),.UNSPECIFIED.,
 .F.,.F.,(4,3,3,3,3,3,3,3,3,3,3,3,3,3,3,3,3,3,3,3,3,3,3,3,3,3,3,3,3,3,3,
3,3,3,3,3,3,3,3,3,3,3,3,3,3,3,3,3,3,3,3,3,3,3,3,3,3,3,3,3,3,3,3,3,3,3,3,
3,3,3,3,3,3,3,3,3,3,3,3,3,3,4),(-613.561516545257,-613.442298360645,-613.375870350287,
-613.295905391501,-613.216034803397,-613.136241066371,-613.056506721281,
-612.976814355976,-612.897135137436,-612.817459373648,-612.737771341781,
-612.658055314671,-612.578251751741,-612.498399027065,-612.418432617415,
-612.376886848088,-612.2969218893,-612.217051301196,-612.137257564168,-612.057523219077,
-611.97783085377,-611.898151635228,-611.818475871439,-611.738787839571,
-611.659071812459,-611.579268249528,-611.49941552485,-611.419449115199,
-611.377903345889,-611.297938387101,-611.218067798997,-611.13827406197,
-611.058539716878,-610.978847351571,-610.89916813303,-610.81949236924,-610.739804337372,
-610.660088310261,-610.58028474733,-610.500432022652,-610.420465613001,
-610.378919843689,-610.298954884902,-610.219084296797,-610.13929055977,
-610.059556214679,-609.979863849373,-609.900184630831,-609.820508867042,
-609.740820835175,-609.661104808063,-609.581301245133,-609.501448520455,
-609.421482110805,-609.37993634149,-609.299971382703,-609.220100794598,
-609.140307057571,-609.06057271248,-608.980880347173,-608.901201128632,
-608.821525364843,-608.741837332975,-608.662121305864,-608.582317742933,
-608.502465018256,-608.422498608605,-608.380952839291,-608.300987880504,
-608.221117292399,-608.141323555372,-608.061589210281,-607.981896844975,
-607.902217626433,-607.822541862644,-607.742853830776,-607.663137803665,
-607.583334240735,-607.503481516057,-607.423515106406,-607.381969337092,
-607.278331238077),.UNSPECIFIED.);
#214=B_SPLINE_CURVE_WITH_KNOTS('',3,(#18063,#18064,#18065,#18066,#18067,
#18068,#18069,#18070,#18071,#18072),.UNSPECIFIED.,.F.,.F.,(4,1,1,1,1,1,
1,4),(-607.278322184525,-606.382985834893,-605.384002332694,-604.385018830495,
-603.386035328296,-602.387051826096,-601.388068323897,-600.995145930897),
 .UNSPECIFIED.);
#215=B_SPLINE_CURVE_WITH_KNOTS('',3,(#18074,#18075,#18076,#18077,#18078,
#18079,#18080,#18081,#18082,#18083),.UNSPECIFIED.,.F.,.F.,(4,1,1,1,1,1,
1,4),(-600.995145930897,-600.389084821698,-599.390101319499,-598.3911178173,
-597.3921343151,-596.393150812901,-595.394167310702,-594.711960623718),
 .UNSPECIFIED.);
#216=B_SPLINE_CURVE_WITH_KNOTS('',3,(#18085,#18086,#18087,#18088,#18089,
#18090,#18091,#18092,#18093,#18094),.UNSPECIFIED.,.F.,.F.,(4,1,1,1,1,1,
1,4),(-594.711960623718,-594.395183808503,-593.396200306304,-592.397216804105,
-591.398233301905,-590.399249799706,-589.400266297507,-588.428775316538),
 .UNSPECIFIED.);
#217=B_SPLINE_CURVE_WITH_KNOTS('',3,(#18096,#18097,#18098,#18099,#18100,
#18101,#18102,#18103,#18104,#18105,#18106,#18107),.UNSPECIFIED.,.F.,.F.,
(4,2,1,1,1,1,1,1,4),(-588.428775316538,-588.401282795308,-587.402299293109,
-586.40331579091,-585.40433228871,-584.405348786511,-583.406365284312,-582.407381782113,
-582.145590009359),.UNSPECIFIED.);
#218=B_SPLINE_CURVE_WITH_KNOTS('',3,(#18109,#18110,#18111,#18112,#18113,
#18114,#18115,#18116,#18117,#18118),.UNSPECIFIED.,.F.,.F.,(4,1,1,1,1,1,
1,4),(-582.145590009359,-581.408398279914,-580.409414777715,-579.410431275515,
-578.411447773316,-577.412464271117,-576.413480768918,-575.862404702179),
 .UNSPECIFIED.);
#219=B_SPLINE_CURVE_WITH_KNOTS('',3,(#18120,#18121,#18122,#18123,#18124,
#18125,#18126,#18127,#18128,#18129),.UNSPECIFIED.,.F.,.F.,(4,1,1,1,1,1,
1,4),(-575.862404702179,-575.414497266719,-574.41551376452,-573.41653026232,
-572.417546760121,-571.418563257922,-570.419579755723,-569.579219395),
 .UNSPECIFIED.);
#220=B_SPLINE_CURVE_WITH_KNOTS('',3,(#18131,#18132,#18133,#18134,#18135,
#18136,#18137,#18138,#18139,#18140,#18141),.UNSPECIFIED.,.F.,.F.,(4,1,1,
1,1,1,1,1,4),(-569.579219395,-569.420596253524,-568.421612751325,-567.422629249126,
-566.423645746926,-565.424662244727,-564.425678742528,-563.426695240329,
-563.29603408782),.UNSPECIFIED.);
#221=B_SPLINE_CURVE_WITH_KNOTS('',3,(#18143,#18144,#18145,#18146,#18147,
#18148,#18149,#18150,#18151,#18152),.UNSPECIFIED.,.F.,.F.,(4,1,1,1,1,1,
1,4),(-563.29603408782,-562.42771173813,-561.428728235931,-560.429744733731,
-559.430761231532,-558.431777729333,-557.432794227134,-557.012848780641),
 .UNSPECIFIED.);
#222=B_SPLINE_CURVE_WITH_KNOTS('',3,(#18154,#18155,#18156,#18157,#18158,
#18159,#18160,#18161,#18162,#18163),.UNSPECIFIED.,.F.,.F.,(4,1,1,1,1,1,
1,4),(-557.012848780641,-556.433810724935,-555.434827222736,-554.435843720536,
-553.436860218337,-552.437876716138,-551.438893213939,-550.729663473461),
 .UNSPECIFIED.);
#223=B_SPLINE_CURVE_WITH_KNOTS('',3,(#18165,#18166,#18167,#18168,#18169,
#18170,#18171,#18172,#18173,#18174,#18175,#18176,#18177,#18178,#18179,#18180,
#18181,#18182,#18183,#18184,#18185,#18186,#18187,#18188,#18189,#18190,#18191,
#18192,#18193,#18194,#18195,#18196,#18197,#18198,#18199,#18200,#18201,#18202,
#18203,#18204,#18205,#18206,#18207,#18208,#18209,#18210,#18211,#18212,#18213,
#18214,#18215,#18216,#18217,#18218,#18219,#18220,#18221,#18222,#18223,#18224,
#18225,#18226,#18227,#18228,#18229,#18230,#18231,#18232,#18233,#18234,#18235,
#18236,#18237,#18238,#18239,#18240,#18241,#18242,#18243,#18244,#18245,#18246,
#18247,#18248,#18249,#18250,#18251,#18252,#18253,#18254,#18255,#18256,#18257,
#18258,#18259,#18260,#18261,#18262,#18263,#18264,#18265,#18266,#18267,#18268,
#18269,#18270,#18271,#18272,#18273,#18274,#18275,#18276,#18277,#18278,#18279,
#18280,#18281,#18282,#18283,#18284,#18285,#18286,#18287,#18288,#18289,#18290,
#18291,#18292,#18293,#18294,#18295,#18296,#18297,#18298,#18299,#18300,#18301,
#18302,#18303,#18304,#18305,#18306,#18307,#18308,#18309,#18310,#18311,#18312,
#18313,#18314,#18315,#18316,#18317,#18318,#18319,#18320,#18321,#18322,#18323,
#18324,#18325,#18326,#18327,#18328,#18329,#18330,#18331,#18332,#18333,#18334,
#18335,#18336,#18337,#18338,#18339,#18340,#18341,#18342,#18343,#18344,#18345,
#18346,#18347,#18348,#18349,#18350,#18351,#18352,#18353,#18354,#18355,#18356,
#18357,#18358,#18359,#18360,#18361,#18362,#18363,#18364,#18365,#18366,#18367,
#18368,#18369,#18370,#18371,#18372,#18373,#18374,#18375,#18376,#18377,#18378,
#18379,#18380,#18381,#18382,#18383,#18384,#18385,#18386,#18387,#18388,#18389,
#18390,#18391,#18392,#18393,#18394,#18395,#18396,#18397,#18398,#18399,#18400,
#18401,#18402,#18403,#18404,#18405,#18406,#18407,#18408),.UNSPECIFIED.,
 .F.,.F.,(4,3,3,3,3,3,3,3,3,3,3,3,3,3,3,3,3,3,3,3,3,3,3,3,3,3,3,3,3,3,3,
3,3,3,3,3,3,3,3,3,3,3,3,3,3,3,3,3,3,3,3,3,3,3,3,3,3,3,3,3,3,3,3,3,3,3,3,
3,3,3,3,3,3,3,3,3,3,3,3,3,3,4),(-550.729663311796,-550.632575528383,-550.534108600299,
-550.43990971174,-550.359944752953,-550.280074164848,-550.200280427822,
-550.120546082731,-550.040853717424,-549.961174498883,-549.881498735094,
-549.801810703227,-549.722094676115,-549.642291113185,-549.562438388507,
-549.482471978857,-549.440926209541,-549.360961250753,-549.281090662649,
-549.201296925622,-549.12156258053,-549.041870215223,-548.962190996682,
-548.882515232893,-548.802827201024,-548.723111173913,-548.643307610982,
-548.563454886304,-548.483488476653,-548.441942707341,-548.361977748554,
-548.282107160449,-548.202313423422,-548.122579078331,-548.042886713024,
-547.963207494483,-547.883531730693,-547.803843698825,-547.724127671714,
-547.644324108783,-547.564471384105,-547.484504974455,-547.442959205142,
-547.362994246355,-547.28312365825,-547.203329921224,-547.123595576133,
-547.043903210826,-546.964223992285,-546.884548228496,-546.804860196628,
-546.725144169517,-546.645340606587,-546.565487881909,-546.485521472259,
-546.443975702943,-546.364010744156,-546.284140156051,-546.204346419024,
-546.124612073933,-546.044919708626,-545.965240490085,-545.885564726296,
-545.805876694428,-545.726160667317,-545.646357104386,-545.566504379708,
-545.486537970058,-545.444992200744,-545.365034063542,-545.285170294057,
-545.205383365879,-545.125655813102,-545.045970216838,-544.966297734187,
-544.886628672647,-544.806947303307,-544.727237892889,-544.647440945723,
-544.567594784061,-544.487635050059,-544.446478166396),.UNSPECIFIED.);
#224=B_SPLINE_CURVE_WITH_KNOTS('',3,(#18410,#18411,#18412,#18413,#18414,
#18415,#18416,#18417,#18418,#18419,#18420,#18421,#18422,#18423,#18424,#18425,
#18426,#18427,#18428,#18429,#18430,#18431,#18432,#18433,#18434,#18435,#18436,
#18437,#18438,#18439,#18440,#18441,#18442,#18443,#18444,#18445,#18446,#18447,
#18448,#18449,#18450,#18451,#18452,#18453,#18454,#18455,#18456,#18457,#18458,
#18459,#18460,#18461,#18462,#18463,#18464,#18465,#18466,#18467,#18468,#18469,
#18470,#18471,#18472,#18473,#18474,#18475,#18476,#18477,#18478,#18479,#18480,
#18481,#18482,#18483,#18484,#18485,#18486,#18487,#18488,#18489,#18490,#18491,
#18492,#18493,#18494,#18495,#18496,#18497,#18498,#18499,#18500,#18501,#18502,
#18503,#18504,#18505,#18506,#18507,#18508,#18509,#18510,#18511,#18512,#18513,
#18514,#18515,#18516,#18517,#18518,#18519,#18520,#18521,#18522,#18523,#18524,
#18525,#18526,#18527,#18528,#18529,#18530,#18531,#18532,#18533,#18534,#18535,
#18536,#18537,#18538,#18539,#18540,#18541,#18542,#18543,#18544,#18545,#18546,
#18547,#18548,#18549,#18550,#18551,#18552,#18553,#18554,#18555,#18556,#18557,
#18558,#18559,#18560,#18561,#18562,#18563,#18564,#18565,#18566,#18567,#18568,
#18569,#18570,#18571,#18572,#18573,#18574,#18575,#18576,#18577,#18578,#18579,
#18580,#18581,#18582,#18583,#18584,#18585,#18586,#18587,#18588,#18589,#18590,
#18591,#18592,#18593,#18594,#18595,#18596,#18597,#18598,#18599,#18600,#18601,
#18602,#18603,#18604,#18605,#18606,#18607,#18608,#18609,#18610,#18611,#18612,
#18613,#18614,#18615,#18616,#18617,#18618,#18619,#18620,#18621,#18622,#18623,
#18624,#18625,#18626,#18627,#18628,#18629,#18630,#18631,#18632,#18633,#18634,
#18635,#18636,#18637,#18638,#18639,#18640,#18641,#18642,#18643,#18644,#18645,
#18646,#18647,#18648,#18649,#18650,#18651,#18652,#18653),.UNSPECIFIED.,
 .F.,.F.,(4,3,3,3,3,3,3,3,3,3,3,3,3,3,3,3,3,3,3,3,3,3,3,3,3,3,3,3,3,3,3,
3,3,3,3,3,3,3,3,3,3,3,3,3,3,3,3,3,3,3,3,3,3,3,3,3,3,3,3,3,3,3,3,3,3,3,3,
3,3,3,3,3,3,3,3,3,3,3,3,3,3,4),(-544.446478166281,-544.366506366184,-544.286628939455,
-544.206828373337,-544.12708721549,-544.04738806054,-543.967702085404,-543.888019598603,
-543.808324883423,-543.728602218847,-543.648792019597,-543.568932711421,
-543.48895960595,-543.447025196346,-543.367060237558,-543.287189649453,
-543.207395912426,-543.127661567335,-543.047969202028,-542.968289983486,
-542.888614219697,-542.808926187829,-542.729210160717,-542.649406597786,
-542.569553873108,-542.489587463457,-542.448041694146,-542.368076735359,
-542.288206147254,-542.208412410227,-542.128678065136,-542.048985699829,
-541.969306481288,-541.889630717499,-541.809942685631,-541.730226658519,
-541.650423095588,-541.57057037091,-541.49060396126,-541.449058191947,-541.36909323316,
-541.289222645055,-541.209428908029,-541.129694562938,-541.050002197631,
-540.97032297909,-540.890647215301,-540.810959183434,-540.731243156322,
-540.651439593392,-540.571586868714,-540.491620459064,-540.450074689748,
-540.370109730961,-540.290239142856,-540.210445405829,-540.130711060738,
-540.051018695431,-539.97133947689,-539.891663713101,-539.811975681233,
-539.732259654121,-539.652456091191,-539.572603366513,-539.492636956862,
-539.451091187549,-539.371126228762,-539.291255640657,-539.21146190363,
-539.131727558539,-539.052035193232,-538.97235597469,-538.892680210901,
-538.812992179033,-538.733276151922,-538.653472588991,-538.573619864313,
-538.493653454663,-538.45210768535,-538.353290578552,-538.255807107317,
-538.163293018638),.UNSPECIFIED.);
#225=B_SPLINE_CURVE_WITH_KNOTS('',3,(#18655,#18656,#18657,#18658,#18659,
#18660,#18661,#18662,#18663,#18664),.UNSPECIFIED.,.F.,.F.,(4,1,1,1,1,1,
1,4),(-538.163292859102,-537.453124183151,-536.454140680951,-535.455157178752,
-534.456173676553,-533.457190174354,-532.458206672155,-531.880107551922),
 .UNSPECIFIED.);
#226=B_SPLINE_CURVE_WITH_KNOTS('',3,(#18666,#18667,#18668,#18669,#18670,
#18671,#18672,#18673,#18674,#18675),.UNSPECIFIED.,.F.,.F.,(4,1,1,1,1,1,
1,4),(-531.880107551922,-531.459223169956,-530.460239667756,-529.461256165557,
-528.462272663358,-527.463289161159,-526.46430565896,-525.596922244743),
 .UNSPECIFIED.);
#227=B_SPLINE_CURVE_WITH_KNOTS('',3,(#18677,#18678,#18679,#18680,#18681,
#18682,#18683,#18684,#18685,#18686,#18687),.UNSPECIFIED.,.F.,.F.,(4,1,1,
1,1,1,1,1,4),(-525.596922244743,-525.465322156761,-524.466338654561,-523.467355152362,
-522.468371650163,-521.469388147964,-520.470404645765,-519.471421143566,
-519.313736937563),.UNSPECIFIED.);
#228=B_SPLINE_CURVE_WITH_KNOTS('',3,(#18689,#18690,#18691,#18692,#18693,
#18694,#18695,#18696,#18697,#18698),.UNSPECIFIED.,.F.,.F.,(4,1,1,1,1,1,
1,4),(-519.313736937563,-518.472437641366,-517.473454139167,-516.474470636968,
-515.475487134769,-514.47650363257,-513.477520130371,-513.030551630384),
 .UNSPECIFIED.);
#229=B_SPLINE_CURVE_WITH_KNOTS('',3,(#18700,#18701,#18702,#18703,#18704,
#18705,#18706,#18707,#18708,#18709),.UNSPECIFIED.,.F.,.F.,(4,1,1,1,1,1,
1,4),(-513.030551630384,-512.478536628171,-511.479553125972,-510.480569623773,
-509.481586121574,-508.482602619375,-507.483619117176,-506.747366323204),
 .UNSPECIFIED.);
#230=B_SPLINE_CURVE_WITH_KNOTS('',3,(#18711,#18712,#18713,#18714,#18715,
#18716,#18717,#18718,#18719,#18720,#18721),.UNSPECIFIED.,.F.,.F.,(4,1,1,
1,1,1,1,1,4),(-506.747366323204,-506.484635614976,-505.485652112777,-504.486668610578,
-503.487685108379,-502.48870160618,-501.489718103981,-500.490734601782,
-500.464181016024),.UNSPECIFIED.);
#231=B_SPLINE_CURVE_WITH_KNOTS('',3,(#18723,#18724,#18725,#18726,#18727,
#18728,#18729,#18730,#18731,#18732),.UNSPECIFIED.,.F.,.F.,(4,1,1,1,1,1,
1,4),(-500.464181016024,-499.491751099582,-498.492767597383,-497.493784095184,
-496.494800592985,-495.495817090786,-494.496833588587,-494.180995708845),
 .UNSPECIFIED.);
#232=B_SPLINE_CURVE_WITH_KNOTS('',3,(#18734,#18735,#18736,#18737,#18738,
#18739,#18740,#18741,#18742,#18743),.UNSPECIFIED.,.F.,.F.,(4,1,1,1,1,1,
1,4),(-494.180995708845,-493.497850086387,-492.498866584188,-491.499883081989,
-490.50089957979,-489.501916077591,-488.502932575392,-487.897810401665),
 .UNSPECIFIED.);
#233=B_SPLINE_CURVE_WITH_KNOTS('',3,(#18745,#18746,#18747,#18748,#18749,
#18750,#18751,#18752,#18753,#18754),.UNSPECIFIED.,.F.,.F.,(4,1,1,1,1,1,
1,4),(-487.897810401665,-487.503949073192,-486.504965570993,-485.505982068794,
-484.506998566595,-483.508015064396,-482.509031562196,-481.614625094486),
 .UNSPECIFIED.);
#234=B_SPLINE_CURVE_WITH_KNOTS('',3,(#18756,#18757,#18758,#18759,#18760,
#18761,#18762,#18763,#18764,#18765,#18766),.UNSPECIFIED.,.F.,.F.,(4,1,1,
1,1,1,1,1,4),(-481.614625094486,-481.510048059997,-480.511064557798,-479.512081055599,
-478.5130975534,-477.514114051201,-476.515130549001,-475.516147046802,-475.331439787306),
 .UNSPECIFIED.);
#235=B_SPLINE_CURVE_WITH_KNOTS('',3,(#18768,#18769,#18770,#18771,#18772,
#18773,#18774,#18775,#18776,#18777),.UNSPECIFIED.,.F.,.F.,(4,1,1,1,1,1,
1,4),(-475.331439787306,-474.517163544603,-473.518180042404,-472.519196540205,
-471.520213038006,-470.521229535807,-469.522246033607,-469.048254480127),
 .UNSPECIFIED.);
#236=B_SPLINE_CURVE_WITH_KNOTS('',3,(#18779,#18780,#18781,#18782,#18783,
#18784,#18785,#18786,#18787,#18788),.UNSPECIFIED.,.F.,.F.,(4,1,1,1,1,1,
1,4),(-469.048254480127,-468.523262531408,-467.524279029209,-466.52529552701,
-465.526312024811,-464.527328522612,-463.528345020412,-462.765069172947),
 .UNSPECIFIED.);
#237=B_SPLINE_CURVE_WITH_KNOTS('',3,(#18790,#18791,#18792,#18793,#18794,
#18795,#18796,#18797,#18798,#18799,#18800),.UNSPECIFIED.,.F.,.F.,(4,1,1,
1,1,1,1,1,4),(-462.765069172947,-462.529361518213,-461.530378016014,-460.531394513815,
-459.532411011616,-458.533427509417,-457.534444007217,-456.535460505018,
-456.481883865767),.UNSPECIFIED.);
#238=B_SPLINE_CURVE_WITH_KNOTS('',3,(#18802,#18803,#18804,#18805,#18806,
#18807,#18808,#18809,#18810,#18811),.UNSPECIFIED.,.F.,.F.,(4,1,1,1,1,1,
1,4),(-456.481883865767,-455.536477002819,-454.53749350062,-453.538509998421,
-452.539526496222,-451.540542994022,-450.541559491823,-450.198698558588),
 .UNSPECIFIED.);
#239=B_SPLINE_CURVE_WITH_KNOTS('',3,(#18813,#18814,#18815,#18816,#18817,
#18818,#18819,#18820,#18821,#18822),.UNSPECIFIED.,.F.,.F.,(4,1,1,1,1,1,
1,4),(-450.198698558588,-449.542575989624,-448.543592487425,-447.544608985226,
-446.545625483027,-445.546641980827,-444.547658478628,-443.915513251408),
 .UNSPECIFIED.);
#240=B_SPLINE_CURVE_WITH_KNOTS('',3,(#18824,#18825,#18826,#18827,#18828,
#18829,#18830,#18831,#18832,#18833),.UNSPECIFIED.,.F.,.F.,(4,1,1,1,1,1,
1,4),(-443.915513251408,-443.548674976429,-442.54969147423,-441.550707972031,
-440.551724469832,-439.552740967632,-438.553757465433,-437.632327944229),
 .UNSPECIFIED.);
#241=B_SPLINE_CURVE_WITH_KNOTS('',3,(#18835,#18836,#18837,#18838,#18839,
#18840,#18841,#18842,#18843,#18844,#18845,#18846),.UNSPECIFIED.,.F.,.F.,
(4,2,1,1,1,1,1,1,4),(-437.632327944229,-437.554773963234,-436.555790461035,
-435.556806958836,-434.557823456637,-433.558839954437,-432.559856452238,
-431.560872950039,-431.349142637049),.UNSPECIFIED.);
#242=B_SPLINE_CURVE_WITH_KNOTS('',3,(#18848,#18849,#18850,#18851,#18852,
#18853,#18854,#18855,#18856,#18857),.UNSPECIFIED.,.F.,.F.,(4,1,1,1,1,1,
1,4),(-431.349142637049,-430.56188944784,-429.562905945641,-428.563922443442,
-427.564938941242,-426.565955439043,-425.566971936844,-425.06595732987),
 .UNSPECIFIED.);
#243=B_SPLINE_CURVE_WITH_KNOTS('',3,(#18859,#18860,#18861,#18862,#18863,
#18864,#18865,#18866,#18867,#18868),.UNSPECIFIED.,.F.,.F.,(4,1,1,1,1,1,
1,4),(-425.06595732987,-424.567988434645,-423.569004932446,-422.570021430247,
-421.571037928047,-420.572054425848,-419.573070923649,-418.78277202269),
 .UNSPECIFIED.);
#244=B_SPLINE_CURVE_WITH_KNOTS('',3,(#18870,#18871,#18872,#18873,#18874,
#18875,#18876,#18877,#18878,#18879,#18880),.UNSPECIFIED.,.F.,.F.,(4,1,1,
1,1,1,1,1,4),(-418.78277202269,-418.57408742145,-417.575103919251,-416.576120417052,
-415.577136914853,-414.578153412653,-413.579169910454,-412.580186408255,
-412.499586715511),.UNSPECIFIED.);
#245=B_SPLINE_CURVE_WITH_KNOTS('',3,(#18882,#18883,#18884,#18885,#18886,
#18887,#18888,#18889,#18890,#18891),.UNSPECIFIED.,.F.,.F.,(4,1,1,1,1,1,
1,4),(-412.499586715511,-411.581202906056,-410.582219403857,-409.583235901657,
-408.584252399458,-407.585268897259,-406.58628539506,-406.216409056793),
 .UNSPECIFIED.);
#246=B_SPLINE_CURVE_WITH_KNOTS('',3,(#18893,#18894,#18895,#18896,#18897,
#18898,#18899,#18900,#18901,#18902,#18903,#18904,#18905,#18906,#18907,#18908,
#18909,#18910,#18911,#18912,#18913,#18914,#18915,#18916,#18917,#18918,#18919,
#18920,#18921,#18922,#18923,#18924,#18925,#18926,#18927,#18928,#18929,#18930,
#18931,#18932,#18933,#18934,#18935,#18936,#18937,#18938,#18939,#18940,#18941,
#18942,#18943,#18944,#18945,#18946,#18947,#18948,#18949,#18950,#18951,#18952,
#18953,#18954,#18955,#18956,#18957,#18958,#18959,#18960,#18961,#18962,#18963,
#18964,#18965,#18966,#18967,#18968,#18969,#18970,#18971,#18972,#18973,#18974,
#18975,#18976,#18977,#18978,#18979,#18980,#18981,#18982,#18983,#18984,#18985,
#18986,#18987,#18988,#18989,#18990,#18991,#18992,#18993,#18994,#18995,#18996,
#18997,#18998,#18999,#19000,#19001,#19002,#19003,#19004,#19005,#19006,#19007,
#19008,#19009,#19010,#19011,#19012,#19013,#19014,#19015,#19016,#19017,#19018,
#19019,#19020,#19021,#19022,#19023,#19024,#19025,#19026,#19027,#19028,#19029,
#19030,#19031,#19032,#19033,#19034,#19035,#19036,#19037,#19038,#19039,#19040,
#19041,#19042,#19043,#19044,#19045,#19046,#19047,#19048,#19049,#19050,#19051,
#19052,#19053,#19054,#19055,#19056,#19057,#19058,#19059,#19060,#19061,#19062,
#19063,#19064,#19065,#19066,#19067,#19068,#19069,#19070,#19071,#19072,#19073,
#19074,#19075,#19076,#19077,#19078,#19079,#19080,#19081,#19082,#19083,#19084,
#19085,#19086,#19087,#19088,#19089,#19090,#19091,#19092,#19093,#19094,#19095,
#19096,#19097,#19098,#19099,#19100,#19101,#19102,#19103,#19104,#19105,#19106,
#19107,#19108,#19109,#19110,#19111,#19112,#19113,#19114,#19115,#19116,#19117,
#19118,#19119,#19120,#19121,#19122,#19123,#19124,#19125,#19126,#19127,#19128,
#19129,#19130,#19131,#19132,#19133,#19134,#19135,#19136,#19137,#19138,#19139),
 .UNSPECIFIED.,.F.,.F.,(4,3,3,3,3,3,3,3,3,3,3,3,3,3,3,3,3,3,3,3,3,3,3,3,
3,3,3,3,3,3,3,3,3,3,3,3,3,3,3,3,3,3,3,3,3,3,3,3,3,3,3,3,3,3,3,3,3,3,3,3,
3,3,3,3,3,3,3,3,3,3,3,3,3,3,3,3,3,3,3,3,3,3,4),(-406.216401408331,-406.136209553946,
-406.05601375924,-405.975798966752,-405.895550110692,-405.81520058091,-405.73479800545,
-405.654263253984,-405.587301892861,-405.507336934074,-405.427466345969,
-405.347672608942,-405.267938263851,-405.188245898544,-405.108566680002,
-405.028890916213,-404.949202884345,-404.869486857234,-404.789683294303,
-404.709830569625,-404.629864159975,-404.588318390662,-404.508353431875,
-404.42848284377,-404.348689106743,-404.268954761652,-404.189262396345,
-404.109583177804,-404.029907414015,-403.950219382147,-403.870503355036,
-403.790699792105,-403.710847067427,-403.630880657777,-403.589334888463,
-403.509369929676,-403.429499341571,-403.349705604544,-403.269971259453,
-403.190278894146,-403.110599675605,-403.030923911816,-402.951235879948,
-402.871519852837,-402.791716289906,-402.711863565228,-402.631897155578,
-402.590351386263,-402.510386427476,-402.430515839371,-402.350722102344,
-402.270987757253,-402.191295391946,-402.111616173405,-402.031940409616,
-401.952252377748,-401.872536350636,-401.792732787706,-401.712880063028,
-401.632913653377,-401.591367884064,-401.511402925277,-401.431532337173,
-401.351738600146,-401.272004255056,-401.192311889749,-401.112632671208,
-401.032956907419,-400.953268875552,-400.87355284844,-400.79374928551,-400.713896560832,
-400.633930151182,-400.592384381865,-400.509988346776,-400.430067771627,
-400.350223801306,-400.270440715539,-400.190702835088,-400.11098969475,
-400.031290175392,-399.951577741183,-399.933216101151),.UNSPECIFIED.);
#247=B_SPLINE_CURVE_WITH_KNOTS('',3,(#19141,#19142,#19143,#19144,#19145,
#19146,#19147,#19148,#19149,#19150),.UNSPECIFIED.,.F.,.F.,(4,1,1,1,1,1,
1,4),(-399.933208553266,-399.593400879666,-398.594417377467,-397.595433875268,
-396.596450373068,-395.597466870869,-394.59848336867,-393.650030793972),
 .UNSPECIFIED.);
#248=B_SPLINE_CURVE_WITH_KNOTS('',3,(#19152,#19153,#19154,#19155,#19156,
#19157,#19158,#19159,#19160,#19161,#19162),.UNSPECIFIED.,.F.,.F.,(4,1,1,
1,1,1,1,1,4),(-393.650030793972,-393.599499866471,-392.600516364272,-391.601532862073,
-390.602549359873,-389.603565857674,-388.604582355475,-387.605598853276,
-387.366845486792),.UNSPECIFIED.);
#249=B_SPLINE_CURVE_WITH_KNOTS('',3,(#19164,#19165,#19166,#19167,#19168,
#19169,#19170,#19171,#19172,#19173),.UNSPECIFIED.,.F.,.F.,(4,1,1,1,1,1,
1,4),(-387.366845486792,-386.606615351077,-385.607631848878,-384.608648346678,
-383.609664844479,-382.61068134228,-381.611697840081,-381.083660179613),
 .UNSPECIFIED.);
#250=B_SPLINE_CURVE_WITH_KNOTS('',3,(#19175,#19176,#19177,#19178,#19179,
#19180,#19181,#19182,#19183,#19184),.UNSPECIFIED.,.F.,.F.,(4,1,1,1,1,1,
1,4),(-381.083660179613,-380.612714337882,-379.613730835683,-378.614747333483,
-377.615763831284,-376.616780329085,-375.617796826886,-374.800474872433),
 .UNSPECIFIED.);
#251=B_SPLINE_CURVE_WITH_KNOTS('',3,(#19186,#19187,#19188,#19189,#19190,
#19191,#19192,#19193,#19194,#19195,#19196),.UNSPECIFIED.,.F.,.F.,(4,1,1,
1,1,1,1,1,4),(-374.800474872433,-374.618813324687,-373.619829822488,-372.620846320288,
-371.621862818089,-370.62287931589,-369.623895813691,-368.624912311492,
-368.517289565254),.UNSPECIFIED.);
#252=B_SPLINE_CURVE_WITH_KNOTS('',3,(#19198,#19199,#19200,#19201,#19202,
#19203,#19204,#19205,#19206,#19207),.UNSPECIFIED.,.F.,.F.,(4,1,1,1,1,1,
1,4),(-368.517289565254,-367.625928809293,-366.626945307093,-365.627961804894,
-364.628978302695,-363.629994800496,-362.631011298297,-362.234104258074),
 .UNSPECIFIED.);
#253=B_SPLINE_CURVE_WITH_KNOTS('',3,(#19209,#19210,#19211,#19212,#19213,
#19214,#19215,#19216,#19217,#19218),.UNSPECIFIED.,.F.,.F.,(4,1,1,1,1,1,
1,4),(-362.234104258074,-361.632027796098,-360.633044293898,-359.634060791699,
-358.6350772895,-357.636093787301,-356.637110285102,-355.950918950894),
 .UNSPECIFIED.);
#254=B_SPLINE_CURVE_WITH_KNOTS('',3,(#19220,#19221,#19222,#19223,#19224,
#19225,#19226,#19227,#19228,#19229,#19230,#19231,#19232,#19233,#19234,#19235,
#19236,#19237,#19238,#19239,#19240,#19241,#19242,#19243,#19244,#19245,#19246,
#19247,#19248,#19249,#19250,#19251,#19252,#19253,#19254,#19255,#19256,#19257,
#19258,#19259,#19260,#19261,#19262,#19263,#19264,#19265,#19266,#19267,#19268,
#19269,#19270,#19271,#19272,#19273,#19274,#19275,#19276,#19277,#19278,#19279,
#19280,#19281,#19282,#19283,#19284,#19285,#19286,#19287,#19288,#19289,#19290,
#19291,#19292,#19293,#19294,#19295,#19296,#19297,#19298,#19299,#19300,#19301,
#19302,#19303,#19304,#19305,#19306,#19307,#19308,#19309,#19310,#19311,#19312,
#19313,#19314,#19315,#19316,#19317,#19318,#19319,#19320,#19321,#19322,#19323,
#19324,#19325,#19326,#19327,#19328,#19329,#19330,#19331,#19332,#19333,#19334,
#19335,#19336,#19337,#19338,#19339,#19340,#19341,#19342,#19343,#19344,#19345,
#19346,#19347,#19348,#19349,#19350,#19351,#19352,#19353,#19354,#19355,#19356,
#19357,#19358,#19359,#19360,#19361,#19362,#19363,#19364,#19365,#19366,#19367,
#19368,#19369,#19370,#19371,#19372,#19373,#19374,#19375,#19376,#19377,#19378,
#19379,#19380,#19381,#19382,#19383,#19384,#19385,#19386,#19387,#19388,#19389,
#19390,#19391,#19392,#19393,#19394,#19395,#19396,#19397,#19398,#19399,#19400,
#19401,#19402,#19403,#19404,#19405,#19406,#19407,#19408,#19409,#19410,#19411,
#19412,#19413,#19414,#19415,#19416,#19417,#19418,#19419,#19420,#19421,#19422,
#19423,#19424,#19425,#19426,#19427,#19428,#19429,#19430,#19431,#19432,#19433,
#19434,#19435,#19436,#19437,#19438,#19439,#19440,#19441,#19442,#19443,#19444,
#19445,#19446,#19447,#19448,#19449,#19450,#19451,#19452,#19453,#19454,#19455,
#19456,#19457,#19458,#19459,#19460,#19461,#19462,#19463,#19464,#19465,#19466),
 .UNSPECIFIED.,.F.,.F.,(4,3,3,3,3,3,3,3,3,3,3,3,3,3,3,3,3,3,3,3,3,3,3,3,
3,3,3,3,3,3,3,3,3,3,3,3,3,3,3,3,3,3,3,3,3,3,3,3,3,3,3,3,3,3,3,3,3,3,3,3,
3,3,3,3,3,3,3,3,3,3,3,3,3,3,3,3,3,3,3,3,3,3,4),(-355.95091874407,-355.856243657912,
-355.760892553551,-355.664791043618,-355.638126782903,-355.558161824115,
-355.478291236009,-355.398497498981,-355.318763153889,-355.239070788581,
-355.159391570039,-355.079715806248,-355.000027774379,-354.920311747267,
-354.840508184335,-354.760655459656,-354.680689050004,-354.639143280703,
-354.559178321916,-354.479307733811,-354.399513996785,-354.319779651694,
-354.240087286387,-354.160408067846,-354.080732304057,-354.001044272189,
-353.921328245078,-353.841524682147,-353.761671957469,-353.681705547819,
-353.640159778504,-353.560194819717,-353.480324231613,-353.400530494586,
-353.320796149495,-353.241103784188,-353.161424565647,-353.081748801858,
-353.002060769991,-352.92234474288,-352.842541179949,-352.762688455272,
-352.682722045621,-352.641176276305,-352.561211317518,-352.481340729413,
-352.401546992386,-352.321812647295,-352.242120281988,-352.162441063447,
-352.082765299657,-352.003077267789,-351.923361240678,-351.843557677747,
-351.763704953069,-351.683738543418,-351.642192774106,-351.562227815319,
-351.482357227214,-351.402563490187,-351.322829145096,-351.243136779789,
-351.163457561248,-351.083781797459,-351.004093765591,-350.92437773848,
-350.844574175549,-350.764721450872,-350.684755041221,-350.643209271907,
-350.563560272858,-350.484005465922,-350.404527033761,-350.325107222228,
-350.242935524914,-350.163568756537,-350.084203390465,-350.004823439038,
-349.925412908382,-349.845915202241,-349.766365489406,-349.686709081971,
-349.667733643715),.UNSPECIFIED.);
#255=B_SPLINE_CURVE_WITH_KNOTS('',3,(#19468,#19469,#19470,#19471,#19472,
#19473,#19474,#19475,#19476,#19477,#19478,#19479),.UNSPECIFIED.,.F.,.F.,
(4,2,1,1,1,1,1,1,4),(-349.667733643715,-349.644225769708,-348.645242267508,
-347.646258765309,-346.64727526311,-345.648291760911,-344.649308258712,
-343.650324756513,-343.384548336535),.UNSPECIFIED.);
#256=B_SPLINE_CURVE_WITH_KNOTS('',3,(#19481,#19482,#19483,#19484,#19485,
#19486,#19487,#19488,#19489,#19490),.UNSPECIFIED.,.F.,.F.,(4,1,1,1,1,1,
1,4),(-343.384548336535,-342.651341254313,-341.652357752114,-340.653374249915,
-339.654390747716,-338.655407245517,-337.656423743318,-337.101363029356),
 .UNSPECIFIED.);
#257=B_SPLINE_CURVE_WITH_KNOTS('',3,(#19492,#19493,#19494,#19495,#19496,
#19497,#19498,#19499,#19500,#19501),.UNSPECIFIED.,.F.,.F.,(4,1,1,1,1,1,
1,4),(-337.101363029356,-336.657440241118,-335.658456738919,-334.65947323672,
-333.660489734521,-332.661506232322,-331.662522730123,-330.818177722176),
 .UNSPECIFIED.);
#258=B_SPLINE_CURVE_WITH_KNOTS('',3,(#19503,#19504,#19505,#19506,#19507,
#19508,#19509,#19510,#19511,#19512,#19513),.UNSPECIFIED.,.F.,.F.,(4,1,1,
1,1,1,1,1,4),(-330.818177722176,-330.663539227923,-329.664555725724,-328.665572223525,
-327.666588721326,-326.667605219127,-325.668621716928,-324.669638214728,
-324.534992414997),.UNSPECIFIED.);
#259=B_SPLINE_CURVE_WITH_KNOTS('',3,(#19515,#19516,#19517,#19518,#19519,
#19520,#19521,#19522,#19523,#19524),.UNSPECIFIED.,.F.,.F.,(4,1,1,1,1,1,
1,4),(-324.534992414997,-323.670654712529,-322.67167121033,-321.672687708131,
-320.673704205932,-319.674720703733,-318.675737201533,-318.251807107817),
 .UNSPECIFIED.);
#260=B_SPLINE_CURVE_WITH_KNOTS('',3,(#19526,#19527,#19528,#19529,#19530,
#19531,#19532,#19533,#19534,#19535),.UNSPECIFIED.,.F.,.F.,(4,1,1,1,1,1,
1,4),(-318.251807107817,-317.676753699334,-316.677770197135,-315.678786694936,
-314.679803192737,-313.680819690538,-312.681836188338,-311.968621800637),
 .UNSPECIFIED.);
#261=B_SPLINE_CURVE_WITH_KNOTS('',3,(#19537,#19538,#19539,#19540,#19541,
#19542,#19543,#19544,#19545,#19546,#19547),.UNSPECIFIED.,.F.,.F.,(4,1,1,
1,1,1,1,1,4),(-311.968621800637,-311.682852686139,-310.68386918394,-309.684885681741,
-308.685902179542,-307.686918677343,-306.687935175144,-305.688951672944,
-305.685436493458),.UNSPECIFIED.);
#262=B_SPLINE_CURVE_WITH_KNOTS('',3,(#19549,#19550,#19551,#19552,#19553,
#19554,#19555,#19556,#19557,#19558,#19559,#19560,#19561,#19562,#19563,#19564,
#19565,#19566,#19567,#19568,#19569,#19570,#19571,#19572,#19573,#19574,#19575,
#19576,#19577,#19578,#19579,#19580,#19581,#19582,#19583,#19584,#19585,#19586,
#19587,#19588,#19589,#19590,#19591,#19592,#19593,#19594,#19595,#19596,#19597,
#19598,#19599,#19600,#19601,#19602,#19603,#19604,#19605,#19606,#19607,#19608,
#19609,#19610,#19611,#19612,#19613,#19614,#19615,#19616,#19617,#19618,#19619,
#19620,#19621,#19622,#19623,#19624,#19625,#19626,#19627,#19628,#19629,#19630,
#19631,#19632,#19633,#19634,#19635,#19636,#19637,#19638,#19639,#19640,#19641,
#19642,#19643,#19644,#19645,#19646,#19647,#19648,#19649,#19650,#19651,#19652,
#19653,#19654,#19655,#19656,#19657,#19658,#19659,#19660,#19661,#19662,#19663,
#19664,#19665,#19666,#19667,#19668,#19669,#19670,#19671,#19672,#19673,#19674,
#19675,#19676,#19677,#19678,#19679,#19680,#19681,#19682,#19683,#19684,#19685,
#19686,#19687,#19688,#19689,#19690,#19691,#19692,#19693,#19694,#19695,#19696,
#19697,#19698,#19699,#19700,#19701,#19702,#19703,#19704,#19705,#19706,#19707,
#19708,#19709,#19710,#19711,#19712,#19713,#19714,#19715,#19716,#19717,#19718,
#19719,#19720,#19721,#19722,#19723,#19724,#19725,#19726,#19727,#19728,#19729,
#19730,#19731,#19732,#19733,#19734,#19735,#19736,#19737,#19738,#19739,#19740,
#19741,#19742,#19743,#19744,#19745,#19746,#19747,#19748,#19749,#19750,#19751,
#19752,#19753,#19754,#19755,#19756,#19757,#19758,#19759,#19760,#19761,#19762,
#19763,#19764,#19765,#19766,#19767,#19768,#19769,#19770,#19771,#19772,#19773,
#19774,#19775,#19776,#19777,#19778,#19779,#19780,#19781,#19782,#19783,#19784,
#19785,#19786,#19787,#19788,#19789,#19790,#19791,#19792),.UNSPECIFIED.,
 .F.,.F.,(4,3,3,3,3,3,3,3,3,3,3,3,3,3,3,3,3,3,3,3,3,3,3,3,3,3,3,3,3,3,3,
3,3,3,3,3,3,3,3,3,3,3,3,3,3,3,3,3,3,3,3,3,3,3,3,3,3,3,3,3,3,3,3,3,3,3,3,
3,3,3,3,3,3,3,3,3,3,3,3,3,3,4),(-305.685436493458,-305.605522177692,-305.525702196027,
-305.445958978862,-305.3662750174,-305.28663285001,-305.207003567203,-305.127377478755,
-305.047738817149,-304.968071810301,-304.888317255143,-304.808513138856,
-304.728596179039,-304.689968170745,-304.610003211958,-304.530132623853,
-304.450338886826,-304.370604541735,-304.290912176428,-304.211232957887,
-304.131557194098,-304.05186916223,-303.972153135118,-303.892349572188,
-303.81249684751,-303.732530437859,-303.690984668546,-303.611019709759,
-303.531149121654,-303.451355384627,-303.371621039536,-303.29192867423,
-303.212249455688,-303.132573691899,-303.052885660032,-302.973169632921,
-302.89336606999,-302.813513345312,-302.733546935662,-302.692001166347,
-302.612036207559,-302.532165619455,-302.452371882428,-302.372637537336,
-302.29294517203,-302.213265953488,-302.133590189699,-302.053902157831,
-301.97418613072,-301.89438256779,-301.814529843111,-301.734563433461,-301.693017664148,
-301.613052705361,-301.533182117256,-301.45338838023,-301.373654035139,
-301.293961669832,-301.214282451291,-301.134606687502,-301.054918655634,
-300.975202628523,-300.895399065592,-300.815546340914,-300.735579931264,
-300.694034161949,-300.614069203162,-300.534198615057,-300.454404878031,
-300.37467053294,-300.294978167632,-300.215298949091,-300.135623185302,
-300.055935153434,-299.976219126323,-299.896415563392,-299.816562838714,
-299.736596429064,-299.695050659749,-299.596740053052,-299.499495703871,
-299.40225135469),.UNSPECIFIED.);
#263=B_SPLINE_CURVE_WITH_KNOTS('',3,(#19794,#19795,#19796,#19797,#19798,
#19799,#19800,#19801,#19802,#19803),.UNSPECIFIED.,.F.,.F.,(4,1,1,1,1,1,
1,4),(-299.402251186278,-298.69606715755,-297.697083655351,-296.698100153152,
-295.699116650953,-294.700133148754,-293.701149646554,-293.119065879099),
 .UNSPECIFIED.);
#264=B_SPLINE_CURVE_WITH_KNOTS('',3,(#19805,#19806,#19807,#19808,#19809,
#19810,#19811,#19812,#19813,#19814,#19815,#19816,#19817,#19818,#19819,#19820,
#19821,#19822,#19823,#19824,#19825,#19826,#19827,#19828,#19829,#19830,#19831,
#19832,#19833,#19834,#19835,#19836,#19837,#19838,#19839,#19840,#19841,#19842,
#19843,#19844,#19845,#19846,#19847,#19848,#19849,#19850,#19851,#19852,#19853,
#19854,#19855,#19856,#19857,#19858,#19859,#19860,#19861,#19862,#19863,#19864,
#19865,#19866,#19867,#19868,#19869,#19870,#19871,#19872,#19873,#19874,#19875,
#19876,#19877,#19878,#19879,#19880,#19881,#19882,#19883,#19884,#19885,#19886,
#19887,#19888,#19889,#19890,#19891,#19892,#19893,#19894,#19895,#19896,#19897,
#19898,#19899,#19900,#19901,#19902,#19903,#19904,#19905,#19906,#19907,#19908,
#19909,#19910,#19911,#19912,#19913,#19914,#19915,#19916,#19917,#19918,#19919,
#19920,#19921,#19922,#19923,#19924,#19925,#19926,#19927,#19928,#19929,#19930,
#19931,#19932,#19933,#19934,#19935,#19936,#19937,#19938,#19939,#19940,#19941,
#19942,#19943,#19944,#19945,#19946,#19947,#19948,#19949,#19950,#19951,#19952,
#19953,#19954,#19955,#19956,#19957,#19958,#19959,#19960,#19961,#19962,#19963,
#19964,#19965,#19966,#19967,#19968,#19969,#19970,#19971,#19972,#19973,#19974,
#19975,#19976,#19977,#19978,#19979,#19980,#19981,#19982,#19983,#19984,#19985,
#19986,#19987,#19988,#19989,#19990,#19991,#19992,#19993,#19994,#19995,#19996,
#19997,#19998,#19999,#20000,#20001,#20002,#20003,#20004,#20005,#20006,#20007,
#20008,#20009,#20010,#20011,#20012,#20013,#20014,#20015,#20016,#20017,#20018,
#20019,#20020,#20021,#20022,#20023,#20024,#20025,#20026,#20027,#20028,#20029,
#20030,#20031,#20032,#20033,#20034,#20035,#20036,#20037,#20038,#20039,#20040,
#20041,#20042,#20043,#20044,#20045,#20046,#20047,#20048),.UNSPECIFIED.,
 .F.,.F.,(4,3,3,3,3,3,3,3,3,3,3,3,3,3,3,3,3,3,3,3,3,3,3,3,3,3,3,3,3,3,3,
3,3,3,3,3,3,3,3,3,3,3,3,3,3,3,3,3,3,3,3,3,3,3,3,3,3,3,3,3,3,3,3,3,3,3,3,
3,3,3,3,3,3,3,3,3,3,3,3,3,3,4),(-293.119065679974,-293.032078649479,-292.944695041724,
-292.8571122961,-292.769227567858,-292.702166144355,-292.622201185568,-292.542330597464,
-292.462536860437,-292.382802515346,-292.30311015004,-292.223430931499,
-292.14375516771,-292.064067135843,-291.984351108732,-291.904547545802,
-291.824694821124,-291.744728411474,-291.703182642156,-291.623217683369,
-291.543347095264,-291.463553358237,-291.383819013146,-291.304126647839,
-291.224447429298,-291.144771665509,-291.065083633641,-290.98536760653,
-290.905564043599,-290.825711318921,-290.745744909271,-290.704199139957,
-290.62423418117,-290.544363593065,-290.464569856038,-290.384835510947,
-290.30514314564,-290.225463927099,-290.14578816331,-290.066100131442,-289.986384104331,
-289.9065805414,-289.826727816722,-289.746761407072,-289.705215637758,-289.625250678971,
-289.545380090866,-289.465586353839,-289.385852008748,-289.306159643442,
-289.2264804249,-289.146804661111,-289.067116629244,-288.987400602132,-288.907597039202,
-288.827744314524,-288.747777904873,-288.706232135559,-288.626267176772,
-288.546396588667,-288.46660285164,-288.386868506549,-288.307176141241,
-288.2274969227,-288.147821158911,-288.068133127043,-287.988417099931,-287.908613537,
-287.828760812322,-287.748794402672,-287.707248633359,-287.628408648173,
-287.549662294741,-287.470991132852,-287.391602312736,-287.313022569158,
-287.234458300051,-287.155892977823,-287.075889876347,-286.997239478252,
-286.916560025085,-286.835880571919),.UNSPECIFIED.);
#265=B_SPLINE_CURVE_WITH_KNOTS('',3,(#20050,#20051,#20052,#20053,#20054,
#20055,#20056,#20057,#20058,#20059,#20060),.UNSPECIFIED.,.F.,.F.,(4,1,1,
1,1,1,1,1,4),(-286.835880571919,-286.70826513116,-285.709281628961,-284.710298126762,
-283.711314624563,-282.712331122364,-281.713347620164,-280.714364117965,
-280.55269526474),.UNSPECIFIED.);
#266=B_SPLINE_CURVE_WITH_KNOTS('',3,(#20062,#20063,#20064,#20065,#20066,
#20067,#20068,#20069,#20070,#20071),.UNSPECIFIED.,.F.,.F.,(4,1,1,1,1,1,
1,4),(-280.55269526474,-279.715380615766,-278.716397113567,-277.717413611368,
-276.718430109169,-275.719446606969,-274.72046310477,-274.26950995756),
 .UNSPECIFIED.);
#267=B_SPLINE_CURVE_WITH_KNOTS('',3,(#20073,#20074,#20075,#20076,#20077,
#20078,#20079,#20080,#20081,#20082),.UNSPECIFIED.,.F.,.F.,(4,1,1,1,1,1,
1,4),(-274.26950995756,-273.721479602571,-272.722496100372,-271.723512598173,
-270.724529095974,-269.725545593774,-268.726562091575,-267.986324650381),
 .UNSPECIFIED.);
#268=B_SPLINE_CURVE_WITH_KNOTS('',3,(#20084,#20085,#20086,#20087,#20088,
#20089,#20090,#20091,#20092,#20093,#20094,#20095,#20096,#20097,#20098,#20099,
#20100,#20101,#20102,#20103,#20104,#20105,#20106,#20107,#20108,#20109,#20110,
#20111,#20112,#20113,#20114,#20115,#20116,#20117,#20118,#20119,#20120,#20121,
#20122,#20123,#20124,#20125,#20126,#20127,#20128,#20129,#20130,#20131,#20132,
#20133,#20134,#20135,#20136,#20137,#20138,#20139,#20140,#20141,#20142,#20143,
#20144,#20145,#20146,#20147,#20148,#20149,#20150,#20151,#20152,#20153,#20154,
#20155,#20156,#20157,#20158,#20159,#20160,#20161,#20162,#20163,#20164,#20165,
#20166,#20167,#20168,#20169,#20170,#20171,#20172,#20173,#20174,#20175,#20176,
#20177,#20178,#20179,#20180,#20181,#20182,#20183,#20184,#20185,#20186,#20187,
#20188,#20189,#20190,#20191,#20192,#20193,#20194,#20195,#20196,#20197,#20198,
#20199,#20200,#20201,#20202,#20203,#20204,#20205,#20206,#20207,#20208,#20209,
#20210,#20211,#20212,#20213,#20214,#20215,#20216,#20217,#20218,#20219,#20220,
#20221,#20222,#20223,#20224,#20225,#20226,#20227,#20228,#20229,#20230,#20231,
#20232,#20233,#20234,#20235,#20236,#20237,#20238,#20239,#20240,#20241,#20242,
#20243,#20244,#20245,#20246,#20247,#20248,#20249,#20250,#20251,#20252,#20253,
#20254,#20255,#20256,#20257,#20258,#20259,#20260,#20261,#20262,#20263,#20264,
#20265,#20266,#20267,#20268,#20269,#20270,#20271,#20272,#20273,#20274,#20275,
#20276,#20277,#20278,#20279,#20280,#20281,#20282,#20283,#20284,#20285,#20286,
#20287,#20288,#20289,#20290,#20291,#20292,#20293,#20294,#20295,#20296,#20297,
#20298,#20299,#20300,#20301,#20302,#20303,#20304,#20305,#20306,#20307,#20308,
#20309,#20310,#20311,#20312,#20313,#20314,#20315,#20316,#20317,#20318,#20319,
#20320,#20321,#20322,#20323,#20324,#20325,#20326,#20327,#20328,#20329,#20330),
 .UNSPECIFIED.,.F.,.F.,(4,3,3,3,3,3,3,3,3,3,3,3,3,3,3,3,3,3,3,3,3,3,3,3,
3,3,3,3,3,3,3,3,3,3,3,3,3,3,3,3,3,3,3,3,3,3,3,3,3,3,3,3,3,3,3,3,3,3,3,3,
3,3,3,3,3,3,3,3,3,3,3,3,3,3,3,3,3,3,3,3,3,3,4),(-267.986324569519,-267.885288901158,
-267.782255160134,-267.727578589376,-267.647613630589,-267.567743042484,
-267.487949305458,-267.408214960367,-267.328522595061,-267.24884337652,
-267.169167612731,-267.089479580863,-267.009763553751,-266.929959990821,
-266.850107266144,-266.770140856493,-266.728595087177,-266.64863012839,
-266.568759540285,-266.488965803258,-266.409231458167,-266.32953909286,
-266.249859874319,-266.17018411053,-266.090496078662,-266.01078005155,-265.93097648862,
-265.851123763942,-265.771157354291,-265.729611584978,-265.649646626191,
-265.569776038086,-265.48998230106,-265.410247955969,-265.330555590662,
-265.250876372121,-265.171200608332,-265.091512576464,-265.011796549353,
-264.931992986423,-264.852140261745,-264.772173852095,-264.730628082779,
-264.650663123991,-264.570792535887,-264.490998798859,-264.411264453768,
-264.331572088461,-264.25189286992,-264.17221710613,-264.092529074262,-264.01281304715,
-263.933009484219,-263.853156759541,-263.773190349891,-263.731644580579,
-263.651679621792,-263.571809033687,-263.49201529666,-263.412280951569,
-263.332588586262,-263.252909367721,-263.173233603932,-263.093545572064,
-263.013829544952,-262.934025982022,-262.854173257344,-262.774206847693,
-262.73266107838,-262.652696119593,-262.572825531488,-262.493031794462,
-262.413297449371,-262.333605084064,-262.253925865523,-262.174250101734,
-262.094562069866,-262.014846042755,-261.935042479824,-261.855189755146,
-261.775223345496,-261.733677576181,-261.703139343201),.UNSPECIFIED.);
#269=B_SPLINE_CURVE_WITH_KNOTS('',3,(#20332,#20333,#20334,#20335,#20336,
#20337,#20338,#20339,#20340,#20341),.UNSPECIFIED.,.F.,.F.,(4,1,1,1,1,1,
1,4),(-261.703135137337,-260.734694073982,-259.735710571783,-258.736727069584,
-257.737743567384,-256.738760065185,-255.739776562986,-255.419954036021),
 .UNSPECIFIED.);
#270=B_SPLINE_CURVE_WITH_KNOTS('',3,(#20343,#20344,#20345,#20346,#20347,
#20348,#20349,#20350,#20351,#20352),.UNSPECIFIED.,.F.,.F.,(4,1,1,1,1,1,
1,4),(-255.419954036021,-254.740793060787,-253.741809558588,-252.742826056389,
-251.743842554189,-250.74485905199,-249.745875549791,-249.136768728842),
 .UNSPECIFIED.);
#271=B_SPLINE_CURVE_WITH_KNOTS('',3,(#20354,#20355,#20356,#20357,#20358,
#20359,#20360,#20361,#20362,#20363),.UNSPECIFIED.,.F.,.F.,(4,1,1,1,1,1,
1,4),(-249.136768728842,-248.746892047592,-247.747908545393,-246.748925043194,
-245.749941540995,-244.750958038795,-243.751974536596,-242.853592464959),
 .UNSPECIFIED.);
#272=B_SPLINE_CURVE_WITH_KNOTS('',3,(#20365,#20366,#20367,#20368,#20369,
#20370,#20371,#20372,#20373,#20374,#20375,#20376,#20377,#20378,#20379,#20380,
#20381,#20382,#20383,#20384,#20385,#20386,#20387,#20388,#20389,#20390,#20391,
#20392,#20393,#20394,#20395,#20396,#20397,#20398,#20399,#20400,#20401,#20402,
#20403,#20404,#20405,#20406,#20407,#20408,#20409,#20410,#20411,#20412,#20413,
#20414,#20415,#20416,#20417,#20418,#20419,#20420,#20421,#20422,#20423,#20424,
#20425,#20426,#20427,#20428,#20429,#20430,#20431,#20432,#20433,#20434,#20435,
#20436,#20437,#20438,#20439,#20440,#20441,#20442,#20443,#20444,#20445,#20446,
#20447,#20448,#20449,#20450,#20451,#20452,#20453,#20454,#20455,#20456,#20457,
#20458,#20459,#20460,#20461,#20462,#20463,#20464,#20465,#20466,#20467,#20468,
#20469,#20470,#20471,#20472,#20473,#20474,#20475,#20476,#20477,#20478,#20479,
#20480,#20481,#20482,#20483,#20484,#20485,#20486,#20487,#20488,#20489,#20490,
#20491,#20492,#20493,#20494,#20495,#20496,#20497,#20498,#20499,#20500,#20501,
#20502,#20503,#20504,#20505,#20506,#20507,#20508,#20509,#20510,#20511,#20512,
#20513,#20514,#20515,#20516,#20517,#20518,#20519,#20520,#20521,#20522,#20523,
#20524,#20525,#20526,#20527,#20528,#20529,#20530,#20531,#20532,#20533,#20534,
#20535,#20536,#20537,#20538,#20539,#20540,#20541,#20542,#20543,#20544,#20545,
#20546,#20547,#20548,#20549,#20550,#20551,#20552,#20553,#20554,#20555,#20556,
#20557,#20558,#20559,#20560,#20561,#20562,#20563,#20564,#20565,#20566,#20567,
#20568,#20569,#20570,#20571,#20572,#20573,#20574,#20575,#20576,#20577,#20578,
#20579,#20580,#20581,#20582,#20583,#20584,#20585,#20586,#20587,#20588,#20589,
#20590,#20591,#20592,#20593,#20594,#20595,#20596,#20597,#20598,#20599,#20600,
#20601,#20602,#20603,#20604,#20605,#20606,#20607,#20608),.UNSPECIFIED.,
 .F.,.F.,(4,3,3,3,3,3,3,3,3,3,3,3,3,3,3,3,3,3,3,3,3,3,3,3,3,3,3,3,3,3,3,
3,3,3,3,3,3,3,3,3,3,3,3,3,3,3,3,3,3,3,3,3,3,3,3,3,3,3,3,3,3,3,3,3,3,3,3,
3,3,3,3,3,3,3,3,3,3,3,3,3,3,4),(-242.853583421662,-242.752991034397,-242.67302607561,
-242.593155487505,-242.513361750478,-242.433627405387,-242.35393504008,
-242.274255821539,-242.19458005775,-242.114892025882,-242.03517599877,-241.95537243584,
-241.875519711162,-241.795553301511,-241.754007532198,-241.674042573411,
-241.594171985306,-241.51437824828,-241.434643903188,-241.354951537882,
-241.275272319341,-241.195596555551,-241.115908523684,-241.036192496572,
-240.956388933642,-240.876536208964,-240.796569799314,-240.755024029999,
-240.675059071211,-240.595188483107,-240.51539474608,-240.435660400988,
-240.355968035681,-240.27628881714,-240.19661305335,-240.116925021482,-240.037208994371,
-239.95740543144,-239.877552706762,-239.797586297111,-239.756040527799,
-239.676075569012,-239.596204980907,-239.51641124388,-239.436676898789,
-239.356984533482,-239.277305314941,-239.197629551152,-239.117941519284,
-239.038225492173,-238.958421929242,-238.878569204564,-238.798602794914,
-238.7570570256,-238.677092066813,-238.597221478708,-238.517427741682,-238.437693396591,
-238.358001031284,-238.278321812743,-238.198646048954,-238.118958017086,
-238.039241989975,-237.959438427045,-237.879585702367,-237.799619292716,
-237.758073523401,-237.678108564614,-237.598237976509,-237.518444239482,
-237.438709894391,-237.359017529084,-237.279338310543,-237.199662546753,
-237.119974514885,-237.040258487774,-236.960454924843,-236.880602200165,
-236.800635790515,-236.759090021202,-236.640918949153,-236.570398114483),
 .UNSPECIFIED.);
#273=B_SPLINE_CURVE_WITH_KNOTS('',3,(#20610,#20611,#20612,#20613,#20614,
#20615,#20616,#20617,#20618,#20619),.UNSPECIFIED.,.F.,.F.,(4,1,1,1,1,1,
1,4),(-236.570393800933,-235.760106519003,-234.761123016804,-233.762139514604,
-232.763156012405,-231.764172510206,-230.765189008007,-230.287212807303),
 .UNSPECIFIED.);
#274=B_SPLINE_CURVE_WITH_KNOTS('',3,(#20621,#20622,#20623,#20624,#20625,
#20626,#20627,#20628,#20629,#20630),.UNSPECIFIED.,.F.,.F.,(4,1,1,1,1,1,
1,4),(-230.287212807303,-229.766205505808,-228.767222003609,-227.76823850141,
-226.76925499921,-225.770271497011,-224.771287994812,-224.004027500124),
 .UNSPECIFIED.);
#275=B_SPLINE_CURVE_WITH_KNOTS('',3,(#20632,#20633,#20634,#20635,#20636,
#20637,#20638,#20639,#20640,#20641,#20642),.UNSPECIFIED.,.F.,.F.,(4,1,1,
1,1,1,1,1,4),(-224.004027500124,-223.772304492613,-222.773320990414,-221.774337488215,
-220.775353986015,-219.776370483816,-218.777386981617,-217.778403479418,
-217.720842192944),.UNSPECIFIED.);
#276=B_SPLINE_CURVE_WITH_KNOTS('',3,(#20644,#20645,#20646,#20647,#20648,
#20649,#20650,#20651,#20652,#20653,#20654,#20655,#20656,#20657,#20658,#20659,
#20660,#20661,#20662,#20663,#20664,#20665,#20666,#20667,#20668,#20669,#20670,
#20671,#20672,#20673,#20674,#20675,#20676,#20677,#20678,#20679,#20680,#20681,
#20682,#20683,#20684,#20685,#20686,#20687,#20688,#20689,#20690,#20691,#20692,
#20693,#20694,#20695,#20696,#20697,#20698,#20699,#20700,#20701,#20702,#20703,
#20704,#20705,#20706,#20707,#20708,#20709,#20710,#20711,#20712,#20713,#20714,
#20715,#20716,#20717,#20718,#20719,#20720,#20721,#20722,#20723,#20724,#20725,
#20726,#20727,#20728,#20729,#20730,#20731,#20732,#20733,#20734,#20735,#20736,
#20737,#20738,#20739,#20740,#20741,#20742,#20743,#20744,#20745,#20746,#20747,
#20748,#20749,#20750,#20751,#20752,#20753,#20754,#20755,#20756,#20757,#20758,
#20759,#20760,#20761,#20762,#20763,#20764,#20765,#20766,#20767,#20768,#20769,
#20770,#20771,#20772,#20773,#20774,#20775,#20776,#20777,#20778,#20779,#20780,
#20781,#20782,#20783,#20784,#20785,#20786,#20787,#20788,#20789,#20790,#20791,
#20792,#20793,#20794,#20795,#20796,#20797,#20798,#20799,#20800,#20801,#20802,
#20803,#20804,#20805,#20806,#20807,#20808,#20809,#20810,#20811,#20812,#20813,
#20814,#20815,#20816,#20817,#20818,#20819,#20820,#20821,#20822,#20823,#20824,
#20825,#20826,#20827,#20828,#20829,#20830,#20831,#20832,#20833,#20834,#20835,
#20836,#20837,#20838,#20839,#20840,#20841,#20842,#20843,#20844,#20845,#20846,
#20847,#20848,#20849,#20850,#20851,#20852,#20853,#20854,#20855,#20856,#20857,
#20858,#20859,#20860,#20861,#20862,#20863,#20864,#20865,#20866,#20867,#20868,
#20869,#20870,#20871,#20872,#20873,#20874,#20875,#20876,#20877,#20878,#20879,
#20880,#20881,#20882,#20883,#20884,#20885,#20886,#20887),.UNSPECIFIED.,
 .F.,.F.,(4,3,3,3,3,3,3,3,3,3,3,3,3,3,3,3,3,3,3,3,3,3,3,3,3,3,3,3,3,3,3,
3,3,3,3,3,3,3,3,3,3,3,3,3,3,3,3,3,3,3,3,3,3,3,3,3,3,3,3,3,3,3,3,3,3,3,3,
3,3,3,3,3,3,3,3,3,3,3,3,3,3,4),(-217.720842192944,-217.641578783107,-217.562406076567,
-217.483305964034,-217.404260401362,-217.325243816638,-217.246240961083,
-217.167235577504,-217.08821140943,-217.00910557981,-216.929957857125,-216.850689582362,
-216.779419977219,-216.699455018432,-216.619584430327,-216.539790693301,
-216.46005634821,-216.380363982903,-216.300684764362,-216.221009000573,
-216.141320968705,-216.061604941594,-215.981801378664,-215.901948653986,
-215.821982244336,-215.78043647502,-215.700471516232,-215.620600928128,
-215.5408071911,-215.461072846009,-215.381380480702,-215.301701262161,-215.222025498371,
-215.142337466503,-215.062621439391,-214.98281787646,-214.902965151782,
-214.822998742131,-214.78145297282,-214.701488014033,-214.621617425928,
-214.541823688901,-214.46208934381,-214.382396978503,-214.302717759962,
-214.223041996173,-214.143353964305,-214.063637937194,-213.983834374263,
-213.903981649585,-213.824015239935,-213.782469470621,-213.702504511834,
-213.622633923729,-213.542840186703,-213.463105841612,-213.383413476305,
-213.303734257764,-213.224058493975,-213.144370462107,-213.064654434996,
-212.984850872066,-212.904998147388,-212.825031737738,-212.783485968422,
-212.703521009635,-212.62365042153,-212.543856684503,-212.464122339413,
-212.384429974106,-212.304750755564,-212.225074991775,-212.145386959907,
-212.065670932796,-211.985867369865,-211.906014645187,-211.826048235537,
-211.784502466223,-211.691784045667,-211.599421182378,-211.507751789104,
-211.4376570074),.UNSPECIFIED.);
#277=B_SPLINE_CURVE_WITH_KNOTS('',3,(#20889,#20890,#20891,#20892,#20893,
#20894,#20895,#20896,#20897,#20898),.UNSPECIFIED.,.F.,.F.,(4,1,1,1,1,1,
1,4),(-211.437656885764,-210.785518964024,-209.786535461825,-208.787551959625,
-207.788568457426,-206.789584955227,-205.790601453028,-205.154471578585),
 .UNSPECIFIED.);
#278=B_SPLINE_CURVE_WITH_KNOTS('',3,(#20900,#20901,#20902,#20903,#20904,
#20905,#20906,#20907,#20908,#20909),.UNSPECIFIED.,.F.,.F.,(4,1,1,1,1,1,
1,4),(-205.154471578585,-204.791617950829,-203.79263444863,-202.79365094643,
-201.794667444231,-200.795683942032,-199.796700439833,-198.871286271405),
 .UNSPECIFIED.);
#279=B_SPLINE_CURVE_WITH_KNOTS('',3,(#20911,#20912,#20913,#20914,#20915,
#20916,#20917,#20918,#20919,#20920,#20921,#20922),.UNSPECIFIED.,.F.,.F.,
(4,2,1,1,1,1,1,1,4),(-198.871286271405,-198.797716937634,-197.798733435435,
-196.799749933235,-195.800766431036,-194.801782928837,-193.802799426638,
-192.803815924439,-192.588100964226),.UNSPECIFIED.);
#280=B_SPLINE_CURVE_WITH_KNOTS('',3,(#20924,#20925,#20926,#20927,#20928,
#20929,#20930,#20931,#20932,#20933,#20934,#20935,#20936,#20937,#20938,#20939,
#20940,#20941,#20942,#20943,#20944,#20945,#20946,#20947,#20948,#20949,#20950,
#20951,#20952,#20953,#20954,#20955,#20956,#20957,#20958,#20959,#20960,#20961,
#20962,#20963,#20964,#20965,#20966,#20967,#20968,#20969,#20970,#20971,#20972,
#20973,#20974,#20975,#20976,#20977,#20978,#20979,#20980,#20981,#20982,#20983,
#20984,#20985,#20986,#20987,#20988,#20989,#20990,#20991,#20992,#20993,#20994,
#20995,#20996,#20997,#20998,#20999,#21000,#21001,#21002,#21003,#21004,#21005,
#21006,#21007,#21008,#21009,#21010,#21011,#21012,#21013,#21014,#21015,#21016,
#21017,#21018,#21019,#21020,#21021,#21022,#21023,#21024,#21025,#21026,#21027,
#21028,#21029,#21030,#21031,#21032,#21033,#21034,#21035,#21036,#21037,#21038,
#21039,#21040,#21041,#21042,#21043,#21044,#21045,#21046,#21047,#21048,#21049,
#21050,#21051,#21052,#21053,#21054,#21055,#21056,#21057,#21058,#21059,#21060,
#21061,#21062,#21063,#21064,#21065,#21066,#21067,#21068,#21069,#21070,#21071,
#21072,#21073,#21074,#21075,#21076,#21077,#21078,#21079,#21080,#21081,#21082,
#21083,#21084,#21085,#21086,#21087,#21088,#21089,#21090,#21091,#21092,#21093,
#21094,#21095,#21096,#21097,#21098,#21099,#21100,#21101,#21102,#21103,#21104,
#21105,#21106,#21107,#21108,#21109,#21110,#21111,#21112,#21113,#21114,#21115,
#21116,#21117,#21118,#21119,#21120,#21121,#21122,#21123,#21124,#21125,#21126,
#21127,#21128,#21129,#21130,#21131,#21132,#21133,#21134,#21135,#21136,#21137,
#21138,#21139,#21140,#21141,#21142,#21143,#21144,#21145,#21146,#21147,#21148,
#21149,#21150,#21151,#21152,#21153,#21154,#21155,#21156,#21157,#21158,#21159,
#21160,#21161,#21162,#21163,#21164,#21165,#21166,#21167),.UNSPECIFIED.,
 .F.,.F.,(4,3,3,3,3,3,3,3,3,3,3,3,3,3,3,3,3,3,3,3,3,3,3,3,3,3,3,3,3,3,3,
3,3,3,3,3,3,3,3,3,3,3,3,3,3,3,3,3,3,3,3,3,3,3,3,3,3,3,3,3,3,3,3,3,3,3,3,
3,3,3,3,3,3,3,3,3,3,3,3,3,3,4),(-192.588100964226,-192.509400610385,-192.430759171616,
-192.35215227097,-192.273562537089,-192.194973453373,-192.116368505404,
-192.037684617319,-191.958960970888,-191.880116824502,-191.80483242224,
-191.724867463453,-191.644996875348,-191.565203138321,-191.485468793229,
-191.405776427922,-191.326097209381,-191.246421445591,-191.166733413723,
-191.087017386612,-191.007213823681,-190.927361099003,-190.847394689352,
-190.80584892004,-190.725883961253,-190.646013373148,-190.566219636121,
-190.48648529103,-190.406792925724,-190.327113707182,-190.247437943393,
-190.167749911525,-190.088033884414,-190.008230321483,-189.928377596805,
-189.848411187154,-189.806865417841,-189.726900459054,-189.647029870949,
-189.567236133923,-189.487501788832,-189.407809423524,-189.328130204983,
-189.248454441194,-189.168766409327,-189.089050382215,-189.009246819285,
-188.929394094607,-188.849427684957,-188.807881915642,-188.727916956855,
-188.64804636875,-188.568252631723,-188.488518286632,-188.408825921325,
-188.329146702783,-188.249470938994,-188.169782907126,-188.090066880015,
-188.010263317085,-187.930410592407,-187.850444182757,-187.808898413443,
-187.728933454656,-187.649062866551,-187.569269129524,-187.489534784433,
-187.409842419126,-187.330163200585,-187.250487436796,-187.170799404927,
-187.091083377816,-187.011279814885,-186.931427090208,-186.851460680557,
-186.809914911244,-186.726038212122,-186.642296982965,-186.557951651485,
-186.474498477817,-186.389707067432,-186.304915657046),.UNSPECIFIED.);
#281=B_SPLINE_CURVE_WITH_KNOTS('',3,(#21169,#21170,#21171,#21172,#21173,
#21174,#21175,#21176,#21177,#21178,#21179,#21180,#21181,#21182,#21183,#21184,
#21185,#21186,#21187,#21188,#21189,#21190,#21191,#21192,#21193,#21194,#21195,
#21196,#21197,#21198,#21199,#21200,#21201,#21202,#21203,#21204,#21205,#21206,
#21207,#21208,#21209,#21210,#21211,#21212,#21213,#21214,#21215,#21216,#21217,
#21218,#21219,#21220,#21221,#21222,#21223,#21224,#21225,#21226,#21227,#21228,
#21229,#21230,#21231,#21232,#21233,#21234,#21235,#21236,#21237,#21238,#21239,
#21240,#21241,#21242,#21243,#21244,#21245,#21246,#21247,#21248,#21249,#21250,
#21251,#21252,#21253,#21254,#21255,#21256,#21257,#21258,#21259,#21260,#21261,
#21262,#21263,#21264,#21265,#21266,#21267,#21268,#21269,#21270,#21271,#21272,
#21273,#21274,#21275,#21276,#21277,#21278,#21279,#21280,#21281,#21282,#21283,
#21284,#21285,#21286,#21287,#21288,#21289,#21290,#21291,#21292,#21293,#21294,
#21295,#21296,#21297,#21298,#21299,#21300,#21301,#21302,#21303,#21304,#21305,
#21306,#21307,#21308,#21309,#21310,#21311,#21312,#21313,#21314,#21315,#21316,
#21317,#21318,#21319,#21320,#21321,#21322,#21323,#21324,#21325,#21326,#21327,
#21328,#21329,#21330,#21331,#21332,#21333,#21334,#21335,#21336,#21337,#21338,
#21339,#21340,#21341,#21342,#21343,#21344,#21345,#21346,#21347,#21348,#21349,
#21350,#21351,#21352,#21353,#21354,#21355,#21356,#21357,#21358,#21359,#21360,
#21361,#21362,#21363,#21364,#21365,#21366,#21367,#21368,#21369,#21370,#21371,
#21372,#21373,#21374,#21375,#21376,#21377,#21378,#21379,#21380,#21381,#21382,
#21383,#21384,#21385,#21386,#21387,#21388,#21389,#21390,#21391,#21392,#21393,
#21394,#21395,#21396,#21397,#21398,#21399,#21400,#21401,#21402,#21403,#21404,
#21405,#21406,#21407,#21408,#21409,#21410,#21411,#21412),.UNSPECIFIED.,
 .F.,.F.,(4,3,3,3,3,3,3,3,3,3,3,3,3,3,3,3,3,3,3,3,3,3,3,3,3,3,3,3,3,3,3,
3,3,3,3,3,3,3,3,3,3,3,3,3,3,3,3,3,3,3,3,3,3,3,3,3,3,3,3,3,3,3,3,3,3,3,3,
3,3,3,3,3,3,3,3,3,3,3,3,3,3,4),(-186.304915656926,-186.221262094494,-186.137497127184,
-186.053532146919,-185.969464210991,-185.885200182465,-185.810931409045,
-185.730966450257,-185.651095862153,-185.571302125125,-185.491567780034,
-185.411875414727,-185.332196196186,-185.252520432396,-185.172832400528,
-185.093116373417,-185.013312810486,-184.933460085808,-184.853493676157,
-184.811947906845,-184.731982948058,-184.652112359953,-184.572318622926,
-184.492584277835,-184.412891912528,-184.333212693987,-184.253536930198,
-184.17384889833,-184.094132871219,-184.014329308288,-183.93447658361,-183.85451017396,
-183.812964404646,-183.732999445859,-183.653128857754,-183.573335120728,
-183.493600775637,-183.41390841033,-183.334229191789,-183.254553428,-183.174865396132,
-183.095149369021,-183.015345806091,-182.935493081413,-182.855526671762,
-182.813980902447,-182.73401594366,-182.654145355555,-182.574351618528,
-182.494617273437,-182.41492490813,-182.335245689589,-182.2555699258,-182.175881893932,
-182.09616586682,-182.01636230389,-181.936509579212,-181.856543169561,-181.814997400248,
-181.735032441461,-181.655161853356,-181.575368116329,-181.495633771238,
-181.415941405931,-181.33626218739,-181.256586423601,-181.176898391733,
-181.097182364622,-181.017378801691,-180.937526077013,-180.857559667363,
-180.816013898049,-180.737185977964,-180.658452667959,-180.578862378197,
-180.500268342106,-180.421707645983,-180.343163738494,-180.262805391337,
-180.184219816278,-180.102975083072,-180.021730349867),.UNSPECIFIED.);
#282=B_SPLINE_CURVE_WITH_KNOTS('',3,(#21414,#21415,#21416,#21417,#21418,
#21419,#21420,#21421,#21422,#21423,#21424),.UNSPECIFIED.,.F.,.F.,(4,1,1,
1,1,1,1,1,4),(-180.021730349867,-179.81703039585,-178.81804689365,-177.819063391451,
-176.820079889252,-175.821096387053,-174.822112884854,-173.823129382655,
-173.738545042687),.UNSPECIFIED.);
#283=B_SPLINE_CURVE_WITH_KNOTS('',3,(#21426,#21427,#21428,#21429,#21430,
#21431,#21432,#21433,#21434,#21435),.UNSPECIFIED.,.F.,.F.,(4,1,1,1,1,1,
1,4),(-173.738545042687,-172.824145880455,-171.825162378256,-170.826178876057,
-169.827195373858,-168.828211871659,-167.82922836946,-167.455367342988),
 .UNSPECIFIED.);
#284=B_SPLINE_CURVE_WITH_KNOTS('',3,(#21437,#21438,#21439,#21440,#21441,
#21442,#21443,#21444,#21445,#21446,#21447,#21448,#21449,#21450,#21451,#21452,
#21453,#21454,#21455,#21456,#21457,#21458,#21459,#21460,#21461,#21462,#21463,
#21464,#21465,#21466,#21467,#21468,#21469,#21470,#21471,#21472,#21473,#21474,
#21475,#21476,#21477,#21478,#21479,#21480,#21481,#21482,#21483,#21484,#21485,
#21486,#21487,#21488,#21489,#21490,#21491,#21492,#21493,#21494,#21495,#21496,
#21497,#21498,#21499,#21500,#21501,#21502,#21503,#21504,#21505,#21506,#21507,
#21508,#21509,#21510,#21511,#21512,#21513,#21514,#21515,#21516,#21517,#21518,
#21519,#21520,#21521,#21522,#21523,#21524,#21525,#21526,#21527,#21528,#21529,
#21530,#21531,#21532,#21533,#21534,#21535,#21536,#21537,#21538,#21539,#21540,
#21541,#21542,#21543,#21544,#21545,#21546,#21547,#21548,#21549,#21550,#21551,
#21552,#21553,#21554,#21555,#21556,#21557,#21558,#21559,#21560,#21561,#21562,
#21563,#21564,#21565,#21566,#21567,#21568,#21569,#21570,#21571,#21572,#21573,
#21574,#21575,#21576,#21577,#21578,#21579,#21580,#21581,#21582,#21583,#21584,
#21585,#21586,#21587,#21588,#21589,#21590,#21591,#21592,#21593,#21594,#21595,
#21596,#21597,#21598,#21599,#21600,#21601,#21602,#21603,#21604,#21605,#21606,
#21607,#21608,#21609,#21610,#21611,#21612,#21613,#21614,#21615,#21616,#21617,
#21618,#21619,#21620,#21621,#21622,#21623,#21624,#21625,#21626,#21627,#21628,
#21629,#21630,#21631,#21632,#21633,#21634,#21635,#21636,#21637,#21638,#21639,
#21640,#21641,#21642,#21643,#21644,#21645,#21646,#21647,#21648,#21649,#21650,
#21651,#21652,#21653,#21654,#21655,#21656,#21657,#21658,#21659,#21660,#21661,
#21662,#21663,#21664,#21665,#21666,#21667,#21668,#21669,#21670,#21671,#21672,
#21673,#21674,#21675,#21676,#21677,#21678,#21679,#21680,#21681,#21682,#21683),
 .UNSPECIFIED.,.F.,.F.,(4,3,3,3,3,3,3,3,3,3,3,3,3,3,3,3,3,3,3,3,3,3,3,3,
3,3,3,3,3,3,3,3,3,3,3,3,3,3,3,3,3,3,3,3,3,3,3,3,3,3,3,3,3,3,3,3,3,3,3,3,
3,3,3,3,3,3,3,3,3,3,3,3,3,3,3,3,3,3,3,3,3,3,4),(-167.455359735507,-167.375098519079,
-167.294831376116,-167.214543341274,-167.13421943968,-167.053793393311,
-166.9733128763,-166.892700782444,-166.830244867261,-166.750279908473,-166.670409320368,
-166.590615583341,-166.510881238249,-166.431188872942,-166.3515096544,-166.271833890611,
-166.192145858742,-166.11242983163,-166.032626268699,-165.952773544021,
-165.87280713437,-165.831261365061,-165.751296406274,-165.671425818169,
-165.591632081142,-165.511897736051,-165.432205370743,-165.352526152202,
-165.272850388413,-165.193162356545,-165.113446329433,-165.033642766502,
-164.953790041824,-164.873823632174,-164.832277862862,-164.752312904075,
-164.672442315971,-164.592648578944,-164.512914233853,-164.433221868547,
-164.353542650006,-164.273866886217,-164.19417885435,-164.114462827238,
-164.034659264308,-163.954806539631,-163.87484012998,-163.833294360663,
-163.753329401876,-163.673458813771,-163.593665076744,-163.513930731653,
-163.434238366346,-163.354559147805,-163.274883384015,-163.195195352147,
-163.115479325036,-163.035675762105,-162.955823037427,-162.875856627777,
-162.834310858464,-162.754345899677,-162.674475311572,-162.594681574545,
-162.514947229455,-162.435254864148,-162.355575645607,-162.275899881818,
-162.19621184995,-162.116495822838,-162.036692259908,-161.95683953523,-161.876873125579,
-161.835327356265,-161.752433240273,-161.672573680655,-161.592790068042,
-161.513066625362,-161.433387616291,-161.353731766857,-161.274088809355,
-161.194430887686,-161.172174428328),.UNSPECIFIED.);
#285=B_SPLINE_CURVE_WITH_KNOTS('',3,(#21685,#21686,#21687,#21688,#21689,
#21690,#21691,#21692,#21693,#21694),.UNSPECIFIED.,.F.,.F.,(4,1,1,1,1,1,
1,4),(-161.172166981905,-160.836343854065,-159.837360351866,-158.838376849667,
-157.839393347468,-156.840409845269,-155.84142634307,-154.888995230419),
 .UNSPECIFIED.);
#286=B_SPLINE_CURVE_WITH_KNOTS('',3,(#21696,#21697,#21698,#21699,#21700,
#21701,#21702,#21703,#21704,#21705,#21706,#21707,#21708,#21709,#21710,#21711,
#21712,#21713,#21714,#21715,#21716,#21717,#21718,#21719,#21720,#21721,#21722,
#21723,#21724,#21725,#21726,#21727,#21728,#21729,#21730,#21731,#21732,#21733,
#21734,#21735,#21736,#21737,#21738,#21739,#21740,#21741,#21742,#21743,#21744,
#21745,#21746,#21747,#21748,#21749,#21750,#21751,#21752,#21753,#21754,#21755,
#21756,#21757,#21758,#21759,#21760,#21761,#21762,#21763,#21764,#21765,#21766,
#21767,#21768,#21769,#21770,#21771,#21772,#21773,#21774,#21775,#21776,#21777,
#21778,#21779,#21780,#21781,#21782,#21783,#21784,#21785,#21786,#21787,#21788,
#21789,#21790,#21791,#21792,#21793,#21794,#21795,#21796,#21797,#21798,#21799,
#21800,#21801,#21802,#21803,#21804,#21805,#21806,#21807,#21808,#21809,#21810,
#21811,#21812,#21813,#21814,#21815,#21816,#21817,#21818,#21819,#21820,#21821,
#21822,#21823,#21824,#21825,#21826,#21827,#21828,#21829,#21830,#21831,#21832,
#21833,#21834,#21835,#21836,#21837,#21838,#21839,#21840,#21841,#21842,#21843,
#21844,#21845,#21846,#21847,#21848,#21849,#21850,#21851,#21852,#21853,#21854,
#21855,#21856,#21857,#21858,#21859,#21860,#21861,#21862,#21863,#21864,#21865,
#21866,#21867,#21868,#21869,#21870,#21871,#21872,#21873,#21874,#21875,#21876,
#21877,#21878,#21879,#21880,#21881,#21882,#21883,#21884,#21885,#21886,#21887,
#21888,#21889,#21890,#21891,#21892,#21893,#21894,#21895,#21896,#21897,#21898,
#21899,#21900,#21901,#21902,#21903,#21904,#21905,#21906,#21907,#21908,#21909,
#21910,#21911,#21912,#21913,#21914,#21915,#21916,#21917,#21918,#21919,#21920,
#21921,#21922,#21923,#21924,#21925,#21926,#21927,#21928,#21929,#21930,#21931,
#21932,#21933,#21934,#21935,#21936,#21937,#21938,#21939,#21940,#21941,#21942),
 .UNSPECIFIED.,.F.,.F.,(4,3,3,3,3,3,3,3,3,3,3,3,3,3,3,3,3,3,3,3,3,3,3,3,
3,3,3,3,3,3,3,3,3,3,3,3,3,3,3,3,3,3,3,3,3,3,3,3,3,3,3,3,3,3,3,3,3,3,3,3,
3,3,3,3,3,3,3,3,3,3,3,3,3,3,3,3,3,3,3,3,3,3,4),(-154.888989121148,-154.84244284087,
-154.762477882083,-154.682607293978,-154.602813556951,-154.52307921186,
-154.443386846553,-154.363707628012,-154.284031864223,-154.204343832355,
-154.124627805244,-154.044824242313,-153.964971517635,-153.885005107985,
-153.843459338671,-153.763494379884,-153.683623791779,-153.603830054752,
-153.524095709661,-153.444403344354,-153.364724125813,-153.285048362024,
-153.205360330156,-153.125644303045,-153.045840740114,-152.965988015436,
-152.886021605786,-152.844475836472,-152.764510877685,-152.68464028958,
-152.604846552553,-152.525112207462,-152.445419842156,-152.365740623614,
-152.286064859825,-152.206376827958,-152.126660800846,-152.046857237916,
-151.967004513238,-151.887038103587,-151.845492334273,-151.765527375486,
-151.685656787381,-151.605863050354,-151.526128705263,-151.446436339956,
-151.366757121415,-151.287081357626,-151.207393325758,-151.127677298646,
-151.047873735716,-150.968021011038,-150.888054601387,-150.846508832074,
-150.766543873287,-150.686673285182,-150.606879548156,-150.527145203065,
-150.447452837758,-150.367773619217,-150.288097855428,-150.20840982356,
-150.128693796449,-150.048890233519,-149.969037508841,-149.88907109919,
-149.847525329875,-149.767560371087,-149.687689782982,-149.607896045955,
-149.528161700864,-149.448469335557,-149.368790117015,-149.289114353226,
-149.209426321358,-149.129710294246,-149.049906731315,-148.970054006637,
-148.890087596986,-148.848541827675,-148.742408125834,-148.638731099375,
-148.605803878848),.UNSPECIFIED.);
#287=B_SPLINE_CURVE_WITH_KNOTS('',3,(#21944,#21945,#21946,#21947,#21948,
#21949,#21950,#21951,#21952,#21953),.UNSPECIFIED.,.F.,.F.,(4,1,1,1,1,1,
1,4),(-148.605803813969,-147.849558325476,-146.850574823277,-145.851591321078,
-144.852607818879,-143.85362431668,-142.854640814481,-142.322618506789),
 .UNSPECIFIED.);
#288=B_SPLINE_CURVE_WITH_KNOTS('',3,(#21955,#21956,#21957,#21958,#21959,
#21960,#21961,#21962,#21963,#21964,#21965,#21966,#21967,#21968,#21969,#21970,
#21971,#21972,#21973,#21974,#21975,#21976,#21977,#21978,#21979,#21980,#21981,
#21982,#21983,#21984,#21985,#21986,#21987,#21988,#21989,#21990,#21991,#21992,
#21993,#21994,#21995,#21996,#21997,#21998,#21999,#22000,#22001,#22002,#22003,
#22004,#22005,#22006,#22007,#22008,#22009,#22010,#22011,#22012,#22013,#22014,
#22015,#22016,#22017,#22018,#22019,#22020,#22021,#22022,#22023,#22024,#22025,
#22026,#22027,#22028,#22029,#22030,#22031,#22032,#22033,#22034,#22035,#22036,
#22037,#22038,#22039,#22040,#22041,#22042,#22043,#22044,#22045,#22046,#22047,
#22048,#22049,#22050,#22051,#22052,#22053,#22054,#22055,#22056,#22057,#22058,
#22059,#22060,#22061,#22062,#22063,#22064,#22065,#22066,#22067,#22068,#22069,
#22070,#22071,#22072,#22073,#22074,#22075,#22076,#22077,#22078,#22079,#22080,
#22081,#22082,#22083,#22084,#22085,#22086,#22087,#22088,#22089,#22090,#22091,
#22092,#22093,#22094,#22095,#22096,#22097,#22098,#22099,#22100,#22101,#22102,
#22103,#22104,#22105,#22106,#22107,#22108,#22109,#22110,#22111,#22112,#22113,
#22114,#22115,#22116,#22117,#22118,#22119,#22120,#22121,#22122,#22123,#22124,
#22125,#22126,#22127,#22128,#22129,#22130,#22131,#22132,#22133,#22134,#22135,
#22136,#22137,#22138,#22139,#22140,#22141,#22142,#22143,#22144,#22145,#22146,
#22147,#22148,#22149,#22150,#22151,#22152,#22153,#22154,#22155,#22156,#22157,
#22158,#22159,#22160,#22161,#22162,#22163,#22164,#22165,#22166,#22167,#22168,
#22169,#22170,#22171,#22172,#22173,#22174,#22175,#22176,#22177,#22178,#22179,
#22180,#22181,#22182,#22183,#22184,#22185,#22186,#22187,#22188,#22189,#22190,
#22191,#22192,#22193,#22194,#22195,#22196,#22197,#22198,#22199,#22200,#22201),
 .UNSPECIFIED.,.F.,.F.,(4,3,3,3,3,3,3,3,3,3,3,3,3,3,3,3,3,3,3,3,3,3,3,3,
3,3,3,3,3,3,3,3,3,3,3,3,3,3,3,3,3,3,3,3,3,3,3,3,3,3,3,3,3,3,3,3,3,3,3,3,
3,3,3,3,3,3,3,3,3,3,3,3,3,3,3,3,3,3,3,3,3,3,4),(-142.322618329037,-142.23793781684,
-142.15310675734,-142.068036935033,-141.982839353648,-141.897437429691,
-141.855657312281,-141.775692353494,-141.695821765389,-141.616028028363,
-141.536293683272,-141.456601317965,-141.376922099424,-141.297246335635,
-141.217558303767,-141.137842276656,-141.058038713725,-140.978185989048,
-140.898219579397,-140.856673810082,-140.776708851295,-140.69683826319,
-140.617044526163,-140.537310181072,-140.457617815765,-140.377938597224,
-140.298262833435,-140.218574801567,-140.138858774456,-140.059055211525,
-139.979202486848,-139.899236077197,-139.857690307883,-139.777725349096,
-139.697854760991,-139.618061023964,-139.538326678873,-139.458634313566,
-139.378955095025,-139.299279331236,-139.219591299368,-139.139875272257,
-139.060071709326,-138.980218984648,-138.900252574998,-138.858706805684,
-138.778741846897,-138.698871258792,-138.619077521765,-138.539343176674,
-138.459650811367,-138.379971592826,-138.300295829037,-138.220607797169,
-138.140891770057,-138.061088207127,-137.981235482449,-137.901269072799,
-137.859723303485,-137.779758344698,-137.699887756593,-137.620094019566,
-137.540359674475,-137.460667309168,-137.380988090627,-137.301312326838,
-137.22162429497,-137.141908267858,-137.062104704928,-136.98225198025,-136.902285570599,
-136.860739801286,-136.781963863931,-136.703281982304,-136.624675669747,
-136.546130316017,-136.467617718984,-136.389121300227,-136.310624495926,
-136.232080347846,-136.153509354394,-136.074858850881,-136.03943319961),
 .UNSPECIFIED.);
#289=B_SPLINE_CURVE_WITH_KNOTS('',3,(#22203,#22204,#22205,#22206,#22207,
#22208,#22209,#22210,#22211,#22212,#22213),.UNSPECIFIED.,.F.,.F.,(4,1,1,
1,1,1,1,1,4),(-136.03943319961,-135.861756299086,-134.862772796887,-133.863789294688,
-132.864805792489,-131.86582229029,-130.866838788091,-129.867855285891,
-129.75624789243),.UNSPECIFIED.);
#290=B_SPLINE_CURVE_WITH_KNOTS('',3,(#22215,#22216,#22217,#22218,#22219,
#22220,#22221,#22222,#22223,#22224,#22225,#22226,#22227,#22228,#22229,#22230,
#22231,#22232,#22233,#22234,#22235,#22236,#22237,#22238,#22239,#22240,#22241,
#22242,#22243,#22244,#22245,#22246,#22247,#22248,#22249,#22250,#22251,#22252,
#22253,#22254,#22255,#22256,#22257,#22258,#22259,#22260,#22261,#22262,#22263,
#22264,#22265,#22266,#22267,#22268,#22269,#22270,#22271,#22272,#22273,#22274,
#22275,#22276,#22277,#22278,#22279,#22280,#22281,#22282,#22283,#22284,#22285,
#22286,#22287,#22288,#22289,#22290,#22291,#22292,#22293,#22294,#22295,#22296,
#22297,#22298,#22299,#22300,#22301,#22302,#22303,#22304,#22305,#22306,#22307,
#22308,#22309,#22310,#22311,#22312,#22313,#22314,#22315,#22316,#22317,#22318,
#22319,#22320,#22321,#22322,#22323,#22324,#22325,#22326,#22327,#22328,#22329,
#22330,#22331,#22332,#22333,#22334,#22335,#22336,#22337,#22338,#22339,#22340,
#22341,#22342,#22343,#22344,#22345,#22346,#22347,#22348,#22349,#22350,#22351,
#22352,#22353,#22354,#22355,#22356,#22357,#22358,#22359,#22360,#22361,#22362,
#22363,#22364,#22365,#22366,#22367,#22368,#22369,#22370,#22371,#22372,#22373,
#22374,#22375,#22376,#22377,#22378,#22379,#22380,#22381,#22382,#22383,#22384,
#22385,#22386,#22387,#22388,#22389,#22390,#22391,#22392,#22393,#22394,#22395,
#22396,#22397,#22398,#22399,#22400,#22401,#22402,#22403,#22404,#22405,#22406,
#22407,#22408,#22409,#22410,#22411,#22412,#22413,#22414,#22415,#22416,#22417,
#22418,#22419,#22420,#22421,#22422,#22423,#22424,#22425,#22426,#22427,#22428,
#22429,#22430,#22431,#22432,#22433,#22434,#22435,#22436,#22437,#22438,#22439,
#22440,#22441,#22442,#22443,#22444,#22445,#22446,#22447,#22448,#22449,#22450,
#22451,#22452,#22453,#22454,#22455,#22456,#22457,#22458,#22459,#22460,#22461),
 .UNSPECIFIED.,.F.,.F.,(4,3,3,3,3,3,3,3,3,3,3,3,3,3,3,3,3,3,3,3,3,3,3,3,
3,3,3,3,3,3,3,3,3,3,3,3,3,3,3,3,3,3,3,3,3,3,3,3,3,3,3,3,3,3,3,3,3,3,3,3,
3,3,3,3,3,3,3,3,3,3,3,3,3,3,3,3,3,3,3,3,3,3,4),(-129.75624789243,-129.677400284394,
-129.598635444903,-129.519935025007,-129.438552119843,-129.359916309128,
-129.281285607269,-129.20264352438,-129.123973564056,-129.04521909352,-128.96641410446,
-128.887503557997,-128.868871783692,-128.788906824905,-128.7090362368,-128.629242499773,
-128.549508154682,-128.469815789375,-128.390136570834,-128.310460807045,
-128.230772775177,-128.151056748066,-128.071253185136,-127.991400460458,
-127.911434050807,-127.869888281493,-127.789923322706,-127.710052734601,
-127.630258997574,-127.550524652483,-127.470832287177,-127.391153068636,
-127.311477304847,-127.231789272979,-127.152073245867,-127.072269682936,
-126.992416958259,-126.912450548608,-126.870904779294,-126.790939820507,
-126.711069232402,-126.631275495375,-126.551541150284,-126.471848784978,
-126.392169566436,-126.312493802647,-126.232805770779,-126.153089743668,
-126.073286180737,-125.993433456059,-125.913467046409,-125.871921277095,
-125.791956318308,-125.712085730203,-125.632291993177,-125.552557648086,
-125.47286528278,-125.393186064239,-125.31351030045,-125.233822268582,-125.15410624147,
-125.07430267854,-124.994449953862,-124.914483544212,-124.872937774896,
-124.792972816109,-124.713102228004,-124.633308490977,-124.553574145886,
-124.473881780578,-124.394202562036,-124.314526798247,-124.234838766379,
-124.155122739268,-124.075319176337,-123.99546645166,-123.915500042009,
-123.873954272696,-123.78504006974,-123.69648948946,-123.608175320554,-123.520245837753,
-123.473062807661),.UNSPECIFIED.);
#291=B_SPLINE_CURVE_WITH_KNOTS('',3,(#22463,#22464,#22465,#22466,#22467,
#22468,#22469,#22470,#22471,#22472),.UNSPECIFIED.,.F.,.F.,(4,1,1,1,1,1,
1,4),(-123.47306258525,-122.874970770497,-121.875987268298,-120.877003766099,
-119.8780202639,-118.879036761701,-117.880053259501,-117.189877278071),
 .UNSPECIFIED.);
#292=B_SPLINE_CURVE_WITH_KNOTS('',3,(#22474,#22475,#22476,#22477,#22478,
#22479,#22480,#22481,#22482,#22483,#22484,#22485,#22486,#22487,#22488,#22489,
#22490,#22491,#22492,#22493,#22494,#22495,#22496,#22497,#22498,#22499,#22500,
#22501,#22502,#22503,#22504,#22505,#22506,#22507,#22508,#22509,#22510,#22511,
#22512,#22513,#22514,#22515,#22516,#22517,#22518,#22519,#22520,#22521,#22522,
#22523,#22524,#22525,#22526,#22527,#22528,#22529,#22530,#22531,#22532,#22533,
#22534,#22535,#22536,#22537,#22538,#22539,#22540,#22541,#22542,#22543,#22544,
#22545,#22546,#22547,#22548,#22549,#22550,#22551,#22552,#22553,#22554,#22555,
#22556,#22557,#22558,#22559,#22560,#22561,#22562,#22563,#22564,#22565,#22566,
#22567,#22568,#22569,#22570,#22571,#22572,#22573,#22574,#22575,#22576,#22577,
#22578,#22579,#22580,#22581,#22582,#22583,#22584,#22585,#22586,#22587,#22588,
#22589,#22590,#22591,#22592,#22593,#22594,#22595,#22596,#22597,#22598,#22599,
#22600,#22601,#22602,#22603,#22604,#22605,#22606,#22607,#22608,#22609,#22610,
#22611,#22612,#22613,#22614,#22615,#22616,#22617,#22618,#22619,#22620,#22621,
#22622,#22623,#22624,#22625,#22626,#22627,#22628,#22629,#22630,#22631,#22632,
#22633,#22634,#22635,#22636,#22637,#22638,#22639,#22640,#22641,#22642,#22643,
#22644,#22645,#22646,#22647,#22648,#22649,#22650,#22651,#22652,#22653,#22654,
#22655,#22656,#22657,#22658,#22659,#22660,#22661,#22662,#22663,#22664,#22665,
#22666,#22667,#22668,#22669,#22670,#22671,#22672,#22673,#22674,#22675,#22676,
#22677,#22678,#22679,#22680,#22681,#22682,#22683,#22684,#22685,#22686,#22687,
#22688,#22689,#22690,#22691,#22692,#22693,#22694,#22695,#22696,#22697,#22698,
#22699,#22700,#22701,#22702,#22703,#22704,#22705,#22706,#22707,#22708,#22709,
#22710,#22711,#22712,#22713,#22714,#22715,#22716,#22717,#22718,#22719,#22720),
 .UNSPECIFIED.,.F.,.F.,(4,3,3,3,3,3,3,3,3,3,3,3,3,3,3,3,3,3,3,3,3,3,3,3,
3,3,3,3,3,3,3,3,3,3,3,3,3,3,3,3,3,3,3,3,3,3,3,3,3,3,3,3,3,3,3,3,3,3,3,3,
3,3,3,3,3,3,3,3,3,3,3,3,3,3,3,3,3,3,3,3,3,3,4),(-117.189877077901,-117.094811079126,
-116.999033985742,-116.902482779177,-116.881069757302,-116.801104798515,
-116.72123421041,-116.641440473384,-116.561706128293,-116.482013762986,
-116.402334544445,-116.322658780656,-116.242970748789,-116.163254721677,
-116.083451158747,-116.003598434069,-115.923632024419,-115.882086255103,
-115.802121296316,-115.722250708211,-115.642456971184,-115.562722626093,
-115.483030260787,-115.403351042245,-115.323675278456,-115.243987246588,
-115.164271219477,-115.084467656547,-115.004614931869,-114.924648522218,
-114.883102752904,-114.803137794117,-114.723267206012,-114.643473468985,
-114.563739123894,-114.484046758587,-114.404367540046,-114.324691776256,
-114.245003744389,-114.165287717277,-114.085484154346,-114.005631429668,
-113.925665020018,-113.884119250705,-113.804154291918,-113.724283703813,
-113.644489966787,-113.564755621696,-113.485063256389,-113.405384037848,
-113.325708274059,-113.246020242191,-113.16630421508,-113.08650065215,-113.006647927472,
-112.926681517822,-112.885135748506,-112.805170789718,-112.725300201614,
-112.645506464586,-112.565772119495,-112.486079754188,-112.406400535647,
-112.326724771857,-112.247036739989,-112.167320712878,-112.087517149947,
-112.007664425269,-111.927698015618,-111.886152246306,-111.806453328173,
-111.726848635618,-111.647320396032,-111.567850899475,-111.485206033402,
-111.405789993568,-111.326375498658,-111.246946600615,-111.16748734538,
-111.087940700449,-111.00834232955,-110.928636233749,-110.906691970891),
 .UNSPECIFIED.);
#293=B_SPLINE_CURVE_WITH_KNOTS('',3,(#22722,#22723,#22724,#22725,#22726,
#22727,#22728,#22729,#22730,#22731,#22732,#22733),.UNSPECIFIED.,.F.,.F.,
(4,2,1,1,1,1,1,1,4),(-110.906691970891,-110.887168744107,-109.888185241908,
-108.889201739709,-107.89021823751,-106.891234735311,-105.892251233111,
-104.893267730912,-104.623510152804),.UNSPECIFIED.);
#294=B_SPLINE_CURVE_WITH_KNOTS('',3,(#22735,#22736,#22737,#22738,#22739,
#22740,#22741,#22742,#22743,#22744,#22745,#22746,#22747,#22748,#22749,#22750,
#22751,#22752,#22753,#22754,#22755,#22756,#22757,#22758,#22759,#22760,#22761,
#22762,#22763,#22764,#22765,#22766,#22767,#22768,#22769,#22770,#22771,#22772,
#22773,#22774,#22775,#22776,#22777,#22778,#22779,#22780,#22781,#22782,#22783,
#22784,#22785,#22786,#22787,#22788,#22789,#22790,#22791,#22792,#22793,#22794,
#22795,#22796,#22797,#22798,#22799,#22800,#22801,#22802,#22803,#22804,#22805,
#22806,#22807,#22808,#22809,#22810,#22811,#22812,#22813,#22814,#22815,#22816,
#22817,#22818,#22819,#22820,#22821,#22822,#22823,#22824,#22825,#22826,#22827,
#22828,#22829,#22830,#22831,#22832,#22833,#22834,#22835,#22836,#22837,#22838,
#22839,#22840,#22841,#22842,#22843,#22844,#22845,#22846,#22847,#22848,#22849,
#22850,#22851,#22852,#22853,#22854,#22855,#22856,#22857,#22858,#22859,#22860,
#22861,#22862,#22863,#22864,#22865,#22866,#22867,#22868,#22869,#22870,#22871,
#22872,#22873,#22874,#22875,#22876,#22877,#22878,#22879,#22880,#22881,#22882,
#22883,#22884,#22885,#22886,#22887,#22888,#22889,#22890,#22891,#22892,#22893,
#22894,#22895,#22896,#22897,#22898,#22899,#22900,#22901,#22902,#22903,#22904,
#22905,#22906,#22907,#22908,#22909,#22910,#22911,#22912,#22913,#22914,#22915,
#22916,#22917,#22918,#22919,#22920,#22921,#22922,#22923,#22924,#22925,#22926,
#22927,#22928,#22929,#22930,#22931,#22932,#22933,#22934,#22935,#22936,#22937,
#22938,#22939,#22940,#22941,#22942,#22943,#22944,#22945,#22946,#22947,#22948,
#22949,#22950,#22951,#22952,#22953,#22954,#22955,#22956,#22957,#22958,#22959,
#22960,#22961,#22962,#22963,#22964,#22965,#22966,#22967,#22968,#22969,#22970,
#22971,#22972,#22973,#22974,#22975,#22976,#22977,#22978,#22979,#22980,#22981),
 .UNSPECIFIED.,.F.,.F.,(4,3,3,3,3,3,3,3,3,3,3,3,3,3,3,3,3,3,3,3,3,3,3,3,
3,3,3,3,3,3,3,3,3,3,3,3,3,3,3,3,3,3,3,3,3,3,3,3,3,3,3,3,3,3,3,3,3,3,3,3,
3,3,3,3,3,3,3,3,3,3,3,3,3,3,3,3,3,3,3,3,3,3,4),(-104.623506663712,-104.544533831671,
-104.463252631302,-104.384335203533,-104.305419740579,-104.226489938422,
-104.143438510995,-104.064388243244,-103.985284593363,-103.906075294704,
-103.894284228713,-103.814319269926,-103.734448681821,-103.654654944795,
-103.574920599704,-103.495228234397,-103.415549015856,-103.335873252067,
-103.256185220199,-103.176469193088,-103.096665630158,-103.01681290548,
-102.936846495829,-102.895300726514,-102.815335767727,-102.735465179622,
-102.655671442595,-102.575937097504,-102.496244732198,-102.416565513657,
-102.336889749868,-102.257201718,-102.177485690888,-102.097682127958,-102.01782940328,
-101.93786299363,-101.896317224315,-101.816352265528,-101.736481677423,
-101.656687940396,-101.576953595305,-101.497261229997,-101.417582011456,
-101.337906247667,-101.258218215799,-101.178502188688,-101.098698625757,
-101.018845901079,-100.938879491428,-100.897333722116,-100.817368763329,
-100.737498175224,-100.657704438197,-100.577970093106,-100.498277727799,
-100.418598509258,-100.338922745469,-100.259234713601,-100.17951868649,
-100.09971512356,-100.019862398881,-99.9398959892309,-99.8983502199165,
-99.8183852611291,-99.7385146730248,-99.6587209359978,-99.5789865909066,
-99.4992942255997,-99.4196150070583,-99.339939243269,-99.2602512114012,
-99.1805351842898,-99.1007316213594,-99.0208788966816,-98.9409124870312,
-98.8993667177173,-98.8172189994476,-98.7351845679469,-98.6532507164691,
-98.5714312330947,-98.4896786671188,-98.4079936626733,-98.3403213565321),
 .UNSPECIFIED.);
#295=B_SPLINE_CURVE_WITH_KNOTS('',3,(#22983,#22984,#22985,#22986,#22987,
#22988,#22989,#22990,#22991,#22992),.UNSPECIFIED.,.F.,.F.,(4,1,1,1,1,1,
1,4),(-98.3403165567537,-97.9003832155181,-96.901399713319,-95.9024162111198,
-94.9034327089206,-93.9044492067215,-92.9054657045223,-92.0571360493525),
 .UNSPECIFIED.);
#296=B_SPLINE_CURVE_WITH_KNOTS('',3,(#22994,#22995,#22996,#22997,#22998,
#22999,#23000,#23001,#23002,#23003,#23004),.UNSPECIFIED.,.F.,.F.,(4,1,1,
1,1,1,1,1,4),(-92.0571360493525,-91.9064822023231,-90.907498700124,-89.9085151979248,
-88.9095316957257,-87.9105481935265,-86.9115646913273,-85.9125811891282,
-85.7739507421729),.UNSPECIFIED.);
#297=B_SPLINE_CURVE_WITH_KNOTS('',3,(#23006,#23007,#23008,#23009,#23010,
#23011,#23012,#23013,#23014,#23015),.UNSPECIFIED.,.F.,.F.,(4,1,1,1,1,1,
1,4),(-85.7739507421729,-84.913597686929,-83.9146141847298,-82.9156306825307,
-81.9166471803315,-80.9176636781323,-79.9186801759332,-79.4907710080448),
 .UNSPECIFIED.);
#298=B_SPLINE_CURVE_WITH_KNOTS('',3,(#23017,#23018,#23019,#23020,#23021,
#23022,#23023,#23024,#23025,#23026,#23027,#23028,#23029,#23030,#23031,#23032,
#23033,#23034,#23035,#23036,#23037,#23038,#23039,#23040,#23041,#23042,#23043,
#23044,#23045,#23046,#23047,#23048,#23049,#23050,#23051,#23052,#23053,#23054,
#23055,#23056,#23057,#23058,#23059,#23060,#23061,#23062,#23063,#23064,#23065,
#23066,#23067,#23068,#23069,#23070,#23071,#23072,#23073,#23074,#23075,#23076,
#23077,#23078,#23079,#23080,#23081,#23082,#23083,#23084,#23085,#23086,#23087,
#23088,#23089,#23090,#23091,#23092,#23093,#23094,#23095,#23096,#23097,#23098,
#23099,#23100,#23101,#23102,#23103,#23104,#23105,#23106,#23107,#23108,#23109,
#23110,#23111,#23112,#23113,#23114,#23115,#23116,#23117,#23118,#23119,#23120,
#23121,#23122,#23123,#23124,#23125,#23126,#23127,#23128,#23129,#23130,#23131,
#23132,#23133,#23134,#23135,#23136,#23137,#23138,#23139,#23140,#23141,#23142,
#23143,#23144,#23145,#23146,#23147,#23148,#23149,#23150,#23151,#23152,#23153,
#23154,#23155,#23156,#23157,#23158,#23159,#23160,#23161,#23162,#23163,#23164,
#23165,#23166,#23167,#23168,#23169,#23170,#23171,#23172,#23173,#23174,#23175,
#23176,#23177,#23178,#23179,#23180,#23181,#23182,#23183,#23184,#23185,#23186,
#23187,#23188,#23189,#23190,#23191,#23192,#23193,#23194,#23195,#23196,#23197,
#23198,#23199,#23200,#23201,#23202,#23203,#23204,#23205,#23206,#23207,#23208,
#23209,#23210,#23211,#23212,#23213,#23214,#23215,#23216,#23217,#23218,#23219,
#23220,#23221,#23222,#23223,#23224,#23225,#23226,#23227,#23228,#23229,#23230,
#23231,#23232,#23233,#23234,#23235,#23236,#23237,#23238,#23239,#23240,#23241,
#23242,#23243,#23244,#23245,#23246,#23247,#23248,#23249,#23250,#23251,#23252,
#23253,#23254,#23255,#23256,#23257,#23258,#23259,#23260),.UNSPECIFIED.,
 .F.,.F.,(4,3,3,3,3,3,3,3,3,3,3,3,3,3,3,3,3,3,3,3,3,3,3,3,3,3,3,3,3,3,3,
3,3,3,3,3,3,3,3,3,3,3,3,3,3,3,3,3,3,3,3,3,3,3,3,3,3,3,3,3,3,3,3,3,3,3,3,
3,3,3,3,3,3,3,3,3,3,3,3,3,3,4),(-79.4907654349933,-79.4093838734493,-79.3279642298507,
-79.2464934153202,-79.1647942299237,-79.0831339105501,-79.0013201594021,
-78.919696673734,-78.8397317149467,-78.759861126842,-78.680067389815,-78.6003330447239,
-78.5206406794171,-78.4409614608759,-78.3612856970868,-78.2815976652188,
-78.2018816381072,-78.1220780751767,-78.0422253504988,-77.9622589408483,
-77.9207131715348,-77.8407482127475,-77.760877624643,-77.6810838876163,
-77.6013495425248,-77.5216571772175,-77.4419779586762,-77.362302194887,
-77.282614163019,-77.2028981359072,-77.1230945729766,-77.0432418482986,
-76.9632754386482,-76.9217296693357,-76.8417647105485,-76.7618941224439,
-76.6821003854173,-76.6023660403263,-76.5226736750192,-76.4429944564781,
-76.3633186926889,-76.2836306608211,-76.2039146337097,-76.1241110707792,
-76.0442583461009,-75.9642919364505,-75.9227461671365,-75.8427812083493,
-75.7629106202447,-75.6831168832177,-75.6033825381264,-75.5236901728197,
-75.4440109542785,-75.3643351904894,-75.2846471586215,-75.2049311315103,
-75.1251275685798,-75.0452748439019,-74.9653084342515,-74.9237626649374,
-74.8437977061501,-74.7639271180454,-74.6841333810186,-74.6043990359275,
-74.5247066706209,-74.4450274520797,-74.3653516882905,-74.2856636564222,
-74.2059476293107,-74.1261440663803,-74.0462913417027,-73.966324932052,
-73.9247791627382,-73.8454582994504,-73.7657235279958,-73.6865968180439,
-73.6075245531369,-73.5284904554073,-73.4482628735089,-73.3692415196554,
-73.2884108237346,-73.2075801278137),.UNSPECIFIED.);
#299=B_SPLINE_CURVE_WITH_KNOTS('',3,(#23262,#23263,#23264,#23265,#23266,
#23267,#23268,#23269,#23270,#23271,#23272),.UNSPECIFIED.,.F.,.F.,(4,1,1,
1,1,1,1,1,4),(-73.2075756699579,-72.925795660539,-71.9268121583399,-70.9278286561407,
-69.9288451539415,-68.9298616517423,-67.9308781495432,-66.931894647344,
-66.9243948206341),.UNSPECIFIED.);
#300=B_SPLINE_CURVE_WITH_KNOTS('',3,(#23274,#23275,#23276,#23277,#23278,
#23279,#23280,#23281,#23282,#23283,#23284,#23285,#23286,#23287,#23288,#23289,
#23290,#23291,#23292,#23293,#23294,#23295,#23296,#23297,#23298,#23299,#23300,
#23301,#23302,#23303,#23304,#23305,#23306,#23307,#23308,#23309,#23310,#23311,
#23312,#23313,#23314,#23315,#23316,#23317,#23318,#23319,#23320,#23321,#23322,
#23323,#23324,#23325,#23326,#23327,#23328,#23329,#23330,#23331,#23332,#23333,
#23334,#23335,#23336,#23337,#23338,#23339,#23340,#23341,#23342,#23343,#23344,
#23345,#23346,#23347,#23348,#23349,#23350,#23351,#23352,#23353,#23354,#23355,
#23356,#23357,#23358,#23359,#23360,#23361,#23362,#23363,#23364,#23365,#23366,
#23367,#23368,#23369,#23370,#23371,#23372,#23373,#23374,#23375,#23376,#23377,
#23378,#23379,#23380,#23381,#23382,#23383,#23384,#23385,#23386,#23387,#23388,
#23389,#23390,#23391,#23392,#23393,#23394,#23395,#23396,#23397,#23398,#23399,
#23400,#23401,#23402,#23403,#23404,#23405,#23406,#23407,#23408,#23409,#23410,
#23411,#23412,#23413,#23414,#23415,#23416,#23417,#23418,#23419,#23420,#23421,
#23422,#23423,#23424,#23425,#23426,#23427,#23428,#23429,#23430,#23431,#23432,
#23433,#23434,#23435,#23436,#23437,#23438,#23439,#23440,#23441,#23442,#23443,
#23444,#23445,#23446,#23447,#23448,#23449,#23450,#23451,#23452,#23453,#23454,
#23455,#23456,#23457,#23458,#23459,#23460,#23461,#23462,#23463,#23464,#23465,
#23466,#23467,#23468,#23469,#23470,#23471,#23472,#23473,#23474,#23475,#23476,
#23477,#23478,#23479,#23480,#23481,#23482,#23483,#23484,#23485,#23486,#23487,
#23488,#23489,#23490,#23491,#23492,#23493,#23494,#23495,#23496,#23497,#23498,
#23499,#23500,#23501,#23502,#23503,#23504,#23505,#23506,#23507,#23508,#23509,
#23510,#23511,#23512,#23513,#23514,#23515,#23516,#23517),.UNSPECIFIED.,
 .F.,.F.,(4,3,3,3,3,3,3,3,3,3,3,3,3,3,3,3,3,3,3,3,3,3,3,3,3,3,3,3,3,3,3,
3,3,3,3,3,3,3,3,3,3,3,3,3,3,3,3,3,3,3,3,3,3,3,3,3,3,3,3,3,3,3,3,3,3,3,3,
3,3,3,3,3,3,3,3,3,3,3,3,3,3,4),(-66.9243948206341,-66.8445366717091,-66.7647727811955,
-66.6850855254513,-66.6054573420193,-66.525870715806,-66.4462966464282,
-66.3667254575869,-66.2871413334151,-66.2075284531903,-66.1278280023542,
-66.0480775294556,-65.9682151673837,-65.9329111451448,-65.8529461863576,
-65.7730755982529,-65.6932818612262,-65.6135475161349,-65.533855150828,
-65.4541759322868,-65.3745001684976,-65.2948121366298,-65.2150961095186,
-65.1352925465881,-65.0554398219102,-64.9754734122598,-64.9339276429457,
-64.8539626841582,-64.7740920960537,-64.6942983590268,-64.6145640139359,
-64.5348716486287,-64.4551924300873,-64.3755166662981,-64.2958286344302,
-64.2161126073187,-64.1363090443881,-64.0564563197102,-63.9764899100596,
-63.9349441407465,-63.8549791819592,-63.7751085938547,-63.6953148568281,
-63.6155805117372,-63.5358881464298,-63.4562089278887,-63.3765331640996,
-63.2968451322321,-63.2171291051206,-63.1373255421901,-63.0574728175123,
-62.977506407862,-62.9359606385474,-62.85599567976,-62.7761250916552,-62.6963313546284,
-62.6165970095373,-62.53690464423,-62.4572254256887,-62.3775496618996,-62.2978616300315,
-62.21814560292,-62.1383420399896,-62.0584893153119,-61.9785229056614,-61.9369771363482,
-61.8570121775608,-61.7771415894564,-61.6973478524296,-61.6176135073379,
-61.5379211420319,-61.4582419234906,-61.3785661597014,-61.2988781278338,
-61.2191621007223,-61.1393585377919,-61.0595058131141,-60.9795394034634,
-60.937993634149,-60.8401739854018,-60.7406918378632,-60.6412096903246),
 .UNSPECIFIED.);
#301=B_SPLINE_CURVE_WITH_KNOTS('',3,(#23519,#23520,#23521,#23522,#23523,
#23524,#23525,#23526,#23527,#23528),.UNSPECIFIED.,.F.,.F.,(4,1,1,1,1,1,
1,4),(-60.6412095134546,-59.9390101319499,-58.9400266297507,-57.9410431275515,
-56.9420596253524,-55.9430761231532,-54.9440926209541,-54.358024206275),
 .UNSPECIFIED.);
#302=B_SPLINE_CURVE_WITH_KNOTS('',3,(#23530,#23531,#23532,#23533,#23534,
#23535,#23536,#23537,#23538,#23539,#23540,#23541,#23542,#23543,#23544,#23545,
#23546,#23547,#23548,#23549,#23550,#23551,#23552,#23553,#23554,#23555,#23556,
#23557,#23558,#23559,#23560,#23561,#23562,#23563,#23564,#23565,#23566,#23567,
#23568,#23569,#23570,#23571,#23572,#23573,#23574,#23575,#23576,#23577,#23578,
#23579,#23580,#23581,#23582,#23583,#23584,#23585,#23586,#23587,#23588,#23589,
#23590,#23591,#23592,#23593,#23594,#23595,#23596,#23597,#23598,#23599,#23600,
#23601,#23602,#23603,#23604,#23605,#23606,#23607,#23608,#23609,#23610,#23611,
#23612,#23613,#23614,#23615,#23616,#23617,#23618,#23619,#23620,#23621,#23622,
#23623,#23624,#23625,#23626,#23627,#23628,#23629,#23630,#23631,#23632,#23633,
#23634,#23635,#23636,#23637,#23638,#23639,#23640,#23641,#23642,#23643,#23644,
#23645,#23646,#23647,#23648,#23649,#23650,#23651,#23652,#23653,#23654,#23655,
#23656,#23657,#23658,#23659,#23660,#23661,#23662,#23663,#23664,#23665,#23666,
#23667,#23668,#23669,#23670,#23671,#23672,#23673,#23674,#23675,#23676,#23677,
#23678,#23679,#23680,#23681,#23682,#23683,#23684,#23685,#23686,#23687,#23688,
#23689,#23690,#23691,#23692,#23693,#23694,#23695,#23696,#23697,#23698,#23699,
#23700,#23701,#23702,#23703,#23704,#23705,#23706,#23707,#23708,#23709,#23710,
#23711,#23712,#23713,#23714,#23715,#23716,#23717,#23718,#23719,#23720,#23721,
#23722,#23723,#23724,#23725,#23726,#23727,#23728,#23729,#23730,#23731,#23732,
#23733,#23734,#23735,#23736,#23737,#23738,#23739,#23740,#23741,#23742,#23743,
#23744,#23745,#23746,#23747,#23748,#23749,#23750,#23751,#23752,#23753,#23754,
#23755,#23756,#23757,#23758,#23759,#23760,#23761,#23762,#23763,#23764,#23765,
#23766,#23767,#23768,#23769,#23770,#23771,#23772,#23773),.UNSPECIFIED.,
 .F.,.F.,(4,3,3,3,3,3,3,3,3,3,3,3,3,3,3,3,3,3,3,3,3,3,3,3,3,3,3,3,3,3,3,
3,3,3,3,3,3,3,3,3,3,3,3,3,3,3,3,3,3,3,3,3,3,3,3,3,3,3,3,3,3,3,3,3,3,3,3,
3,3,3,3,3,3,3,3,3,3,3,3,3,3,4),(-54.3580240007055,-54.2708272108514,-54.1832202248342,
-54.0954065611413,-54.007286490156,-53.9451091187549,-53.8651441599678,
-53.7852735718634,-53.7054798348367,-53.6257454897457,-53.5460531244392,
-53.4663739058981,-53.3866981421091,-53.3070101102414,-53.22729408313,-53.1474905201998,
-53.0676377955221,-52.9876713858718,-52.9461256165557,-52.8661606577684,
-52.7862900696638,-52.7064963326369,-52.6267619875458,-52.5470696222389,
-52.4673904036976,-52.3877146399085,-52.3080266080406,-52.2283105809291,
-52.1485070179987,-52.0686542933208,-51.9886878836703,-51.9471421143566,
-51.8671771555693,-51.7873065674647,-51.7075128304378,-51.6277784853467,
-51.5480861200399,-51.4684069014987,-51.3887311377095,-51.3090431058416,
-51.22932707873,-51.1495235157996,-51.0696707911216,-50.9897043814711,-50.9481586121574,
-50.8681936533701,-50.7883230652655,-50.7085293282386,-50.6287949831475,
-50.5491026178406,-50.4694233992994,-50.3897476355102,-50.3100596036424,
-50.2303435765308,-50.1505400136004,-50.0706872889225,-49.990720879272,
-49.9491751099582,-49.8692101511709,-49.7893395630663,-49.7095458260395,
-49.6298114809484,-49.5501191156415,-49.4704398971003,-49.3907641333111,
-49.3110761014431,-49.2313600743315,-49.151556511401,-49.0717037867231,
-48.9917373770727,-48.9501916077591,-48.8713376044971,-48.7925772262353,
-48.7138920422833,-48.6340103993848,-48.5554166786926,-48.4768383365752,
-48.3982588533269,-48.317403864769,-48.2387381062066,-48.156788502651,-48.0748388990954),
 .UNSPECIFIED.);
#303=B_SPLINE_CURVE_WITH_KNOTS('',3,(#23775,#23776,#23777,#23778,#23779,
#23780,#23781,#23782,#23783,#23784,#23785),.UNSPECIFIED.,.F.,.F.,(4,1,1,
1,1,1,1,1,4),(-48.0748388990954,-47.9512081055599,-46.9522246033607,-45.9532411011616,
-44.9542575989624,-43.9552740967632,-42.9562905945641,-41.9573070923649,
-41.7916535919158),.UNSPECIFIED.);
#304=B_SPLINE_CURVE_WITH_KNOTS('',3,(#23787,#23788,#23789,#23790,#23791,
#23792,#23793,#23794,#23795,#23796),.UNSPECIFIED.,.F.,.F.,(4,1,1,1,1,1,
1,4),(-41.7916535919158,-40.9583235901658,-39.9593400879666,-38.9603565857674,
-37.9613730835683,-36.9623895813691,-35.9634060791699,-35.5084682847362),
 .UNSPECIFIED.);
#305=B_SPLINE_CURVE_WITH_KNOTS('',3,(#23798,#23799,#23800,#23801,#23802,
#23803,#23804,#23805,#23806,#23807),.UNSPECIFIED.,.F.,.F.,(4,1,1,1,1,1,
1,4),(-35.5084682847362,-34.9644225769708,-33.9654390747716,-32.9664555725724,
-31.9674720703733,-30.9684885681741,-29.9695050659749,-29.2252829775566),
 .UNSPECIFIED.);
#306=B_SPLINE_CURVE_WITH_KNOTS('',3,(#23809,#23810,#23811,#23812,#23813,
#23814,#23815,#23816,#23817,#23818,#23819,#23820,#23821,#23822,#23823,#23824,
#23825,#23826,#23827,#23828,#23829,#23830,#23831,#23832,#23833,#23834,#23835,
#23836,#23837,#23838,#23839,#23840,#23841,#23842,#23843,#23844,#23845,#23846,
#23847,#23848,#23849,#23850,#23851,#23852,#23853,#23854,#23855,#23856,#23857,
#23858,#23859,#23860,#23861,#23862,#23863,#23864,#23865,#23866,#23867,#23868,
#23869,#23870,#23871,#23872,#23873,#23874,#23875,#23876,#23877,#23878,#23879,
#23880,#23881,#23882,#23883,#23884,#23885,#23886,#23887,#23888,#23889,#23890,
#23891,#23892,#23893,#23894,#23895,#23896,#23897,#23898,#23899,#23900,#23901,
#23902,#23903,#23904,#23905,#23906,#23907,#23908,#23909,#23910,#23911,#23912,
#23913,#23914,#23915,#23916,#23917,#23918,#23919,#23920,#23921,#23922,#23923,
#23924,#23925,#23926,#23927,#23928,#23929,#23930,#23931,#23932,#23933,#23934,
#23935,#23936,#23937,#23938,#23939,#23940,#23941,#23942,#23943,#23944,#23945,
#23946,#23947,#23948,#23949,#23950,#23951,#23952,#23953,#23954,#23955,#23956,
#23957,#23958,#23959,#23960,#23961,#23962,#23963,#23964,#23965,#23966,#23967,
#23968,#23969,#23970,#23971,#23972,#23973,#23974,#23975,#23976,#23977,#23978,
#23979,#23980,#23981,#23982,#23983,#23984,#23985,#23986,#23987,#23988,#23989,
#23990,#23991,#23992,#23993,#23994,#23995,#23996,#23997,#23998,#23999,#24000,
#24001,#24002,#24003,#24004,#24005,#24006,#24007,#24008,#24009,#24010,#24011,
#24012,#24013,#24014,#24015,#24016,#24017,#24018,#24019,#24020,#24021,#24022,
#24023,#24024,#24025,#24026,#24027,#24028,#24029,#24030,#24031,#24032,#24033,
#24034,#24035,#24036,#24037,#24038,#24039,#24040,#24041,#24042,#24043,#24044,
#24045,#24046,#24047,#24048,#24049,#24050,#24051,#24052,#24053,#24054,#24055),
 .UNSPECIFIED.,.F.,.F.,(4,3,3,3,3,3,3,3,3,3,3,3,3,3,3,3,3,3,3,3,3,3,3,3,
3,3,3,3,3,3,3,3,3,3,3,3,3,3,3,3,3,3,3,3,3,3,3,3,3,3,3,3,3,3,3,3,3,3,3,3,
3,3,3,3,3,3,3,3,3,3,3,3,3,3,3,3,3,3,3,3,3,3,4),(-29.225282908638,-29.1236675299761,
-29.019946111268,-28.9705215637758,-28.8905566050103,-28.8106860169276,
-28.7308922799228,-28.651157934854,-28.5714655695693,-28.4917863510505,
-28.4121105872837,-28.3324225554383,-28.2527065283492,-28.1729029654411,
-28.0930502407854,-28.0130838311569,-27.9715380615766,-27.8915731027056,
-27.8117025145171,-27.7319087774063,-27.6521744322314,-27.5724820668408,
-27.4928028482162,-27.413127084344,-27.3334390523934,-27.2537230251996,
-27.1739194621878,-27.094066737429,-27.0141003276991,-26.9725545593774,
-26.8925896006817,-26.8127190126685,-26.7329252757326,-26.6531909307319,
-26.5734985655149,-26.4938193470624,-26.4141435833613,-26.3344555515808,
-26.2547395245557,-26.17493596171,-26.095083237116,-26.0151168275474,-25.9735710571783,
-25.8936060985027,-25.8137355105109,-25.7339417735978,-25.6542074286215,
-25.5745150634301,-25.4948358450051,-25.4151600813326,-25.3354720495818,
-25.2557560225876,-25.1759524597742,-25.0960997352135,-25.0161333256793,
-24.9745875549791,-24.894622595637,-24.8147520069765,-24.734958269393,-24.6552239237453,
-24.575531557882,-24.495852338787,-24.4161765744455,-24.3364885420273,-24.2567725143677,
-24.176968950896,-24.0971162256796,-24.0171498154998,-23.9756040527799,
-23.8956390947281,-23.8157685073574,-23.7359747710621,-23.6562404266996,
-23.5765480621178,-23.4968688442942,-23.4171930812177,-23.3375050500571,
-23.2577890236469,-23.1779854614052,-23.09813273741,-23.0181663284267,-22.9766205505808,
-22.9420976703771),.UNSPECIFIED.);
#307=B_SPLINE_CURVE_WITH_KNOTS('',3,(#24057,#24058,#24059,#24060,#24061,
#24062,#24063,#24064,#24065,#24066),.UNSPECIFIED.,.F.,.F.,(4,1,1,1,1,1,
1,4),(-22.9420930021365,-21.9776370483816,-20.9786535461825,-19.9796700439833,
-18.9806865417841,-17.981703039585,-16.9827195373858,-16.6589194036327),
 .UNSPECIFIED.);
#308=B_SPLINE_CURVE_WITH_KNOTS('',3,(#24068,#24069,#24070,#24071,#24072,
#24073,#24074,#24075,#24076,#24077,#24078,#24079,#24080,#24081,#24082,#24083,
#24084,#24085,#24086,#24087,#24088,#24089,#24090,#24091,#24092,#24093,#24094,
#24095,#24096,#24097,#24098,#24099,#24100,#24101,#24102,#24103,#24104,#24105,
#24106,#24107,#24108,#24109,#24110,#24111,#24112,#24113,#24114,#24115,#24116,
#24117,#24118,#24119,#24120,#24121,#24122,#24123,#24124,#24125,#24126,#24127,
#24128,#24129,#24130,#24131,#24132,#24133,#24134,#24135,#24136,#24137,#24138,
#24139,#24140,#24141,#24142,#24143,#24144,#24145,#24146,#24147,#24148,#24149,
#24150,#24151,#24152,#24153,#24154,#24155,#24156,#24157,#24158,#24159,#24160,
#24161,#24162,#24163,#24164,#24165,#24166,#24167,#24168,#24169,#24170,#24171,
#24172,#24173,#24174,#24175,#24176,#24177,#24178,#24179,#24180,#24181,#24182,
#24183,#24184,#24185,#24186,#24187,#24188,#24189,#24190,#24191,#24192,#24193,
#24194,#24195,#24196,#24197,#24198,#24199,#24200,#24201,#24202,#24203,#24204,
#24205,#24206,#24207,#24208,#24209,#24210,#24211,#24212,#24213,#24214,#24215,
#24216,#24217,#24218,#24219,#24220,#24221,#24222,#24223,#24224,#24225,#24226,
#24227,#24228,#24229,#24230,#24231,#24232,#24233,#24234,#24235,#24236,#24237,
#24238,#24239,#24240,#24241,#24242,#24243,#24244,#24245,#24246,#24247,#24248,
#24249,#24250,#24251,#24252,#24253,#24254,#24255,#24256,#24257,#24258,#24259,
#24260,#24261,#24262,#24263,#24264,#24265,#24266,#24267,#24268,#24269,#24270,
#24271,#24272,#24273,#24274,#24275,#24276,#24277,#24278,#24279,#24280,#24281,
#24282,#24283,#24284,#24285,#24286,#24287,#24288,#24289,#24290,#24291,#24292,
#24293,#24294,#24295,#24296,#24297,#24298,#24299,#24300,#24301,#24302,#24303,
#24304,#24305,#24306,#24307,#24308,#24309,#24310,#24311,#24312,#24313,#24314),
 .UNSPECIFIED.,.F.,.F.,(4,3,3,3,3,3,3,3,3,3,3,3,3,3,3,3,3,3,3,3,3,3,3,3,
3,3,3,3,3,3,3,3,3,3,3,3,3,3,3,3,3,3,3,3,3,3,3,3,3,3,3,3,3,3,3,3,3,3,3,3,
3,3,3,3,3,3,3,3,3,3,3,3,3,3,3,3,3,3,3,3,3,3,4),(-16.6589123631975,-16.579410177248,
-16.4999164814568,-16.4204232135971,-16.3409145385783,-16.2613746148487,
-16.1817426099068,-16.102058428893,-16.0222573539416,-15.9837360351866,
-15.9037709364464,-15.8239002078398,-15.7441063299001,-15.6643718436215,
-15.5846793369886,-15.5049999773649,-15.4253240726587,-15.3456359001607,
-15.2659197328274,-15.1861160310025,-15.1062631679752,-15.0262966220169,
-14.9847525329875,-14.9047878768464,-14.8249175914123,-14.745124156798,
-14.6653901135813,-14.5856980493307,-14.5060191296772,-14.4263436634018,
-14.3466559274219,-14.2669401943189,-14.1871369210702,-14.1072844840547,
-14.0273183564487,-13.9857690307883,-13.9058039524718,-13.8259332467455,
-13.7461393940897,-13.6664049354483,-13.5867124587574,-13.5070331323954,
-13.4273572630035,-13.3476691278334,-13.2679529998044,-13.1881493400669,
-13.1082965207654,-13.028330020695,-12.9867855285891,-12.9068197350172,
-12.8269483081417,-12.7471537291907,-12.6674185398466,-12.5877253287758,
-12.5080452649217,-12.4283686561855,-12.3486797804667,-12.2689629113326,
-12.1891585134071,-12.1093049564721,-12.0293377260061,-11.98780202639,-11.9078391995772,
-11.8279707447898,-11.7481791404182,-11.6684469253298,-11.5887566853915,
-11.5090795785972,-11.4294059179036,-11.3497199786927,-11.2700060320064,
-11.1902045204954,-11.1103538338639,-11.0303894239007,-10.9888185241908,
-10.9079683874311,-10.8272182709324,-10.7465533331597,-10.6659587888609,
-10.5854271020028,-10.5049324535704,-10.4244554222795,-10.3757270560178),
 .UNSPECIFIED.);
#309=B_SPLINE_CURVE_WITH_KNOTS('',3,(#24315,#24316,#24317,#24318,#24319,
#24320,#24321,#24322,#24323,#24324,#24325,#24326,#24327,#24328,#24329,#24330,
#24331,#24332,#24333,#24334,#24335,#24336,#24337,#24338,#24339,#24340,#24341,
#24342,#24343,#24344,#24345,#24346,#24347,#24348,#24349,#24350,#24351,#24352,
#24353,#24354,#24355,#24356,#24357,#24358,#24359,#24360,#24361,#24362,#24363,
#24364,#24365,#24366,#24367,#24368,#24369,#24370,#24371,#24372,#24373,#24374,
#24375,#24376,#24377,#24378,#24379,#24380,#24381,#24382,#24383,#24384,#24385,
#24386,#24387,#24388,#24389,#24390,#24391,#24392,#24393,#24394,#24395,#24396,
#24397,#24398,#24399,#24400,#24401,#24402,#24403,#24404,#24405,#24406,#24407,
#24408,#24409,#24410,#24411,#24412,#24413,#24414,#24415,#24416,#24417,#24418,
#24419,#24420,#24421,#24422,#24423,#24424,#24425,#24426,#24427,#24428,#24429,
#24430,#24431,#24432,#24433,#24434,#24435,#24436,#24437,#24438,#24439,#24440,
#24441,#24442,#24443,#24444,#24445,#24446,#24447,#24448,#24449,#24450,#24451,
#24452,#24453,#24454,#24455,#24456,#24457,#24458,#24459,#24460,#24461,#24462,
#24463,#24464,#24465,#24466,#24467,#24468,#24469,#24470,#24471,#24472,#24473,
#24474,#24475,#24476,#24477,#24478,#24479,#24480,#24481,#24482,#24483,#24484,
#24485,#24486,#24487,#24488,#24489,#24490,#24491,#24492,#24493,#24494,#24495,
#24496,#24497,#24498,#24499,#24500,#24501,#24502,#24503,#24504,#24505,#24506,
#24507,#24508,#24509,#24510,#24511,#24512,#24513,#24514,#24515,#24516,#24517,
#24518,#24519,#24520,#24521,#24522,#24523,#24524,#24525,#24526,#24527,#24528,
#24529,#24530,#24531,#24532,#24533,#24534,#24535,#24536,#24537,#24538,#24539,
#24540,#24541,#24542,#24543,#24544,#24545,#24546,#24547,#24548,#24549,#24550,
#24551,#24552,#24553,#24554,#24555,#24556,#24557,#24558,#24559,#24560,#24561),
 .UNSPECIFIED.,.F.,.F.,(4,3,3,3,3,3,3,3,3,3,3,3,3,3,3,3,3,3,3,3,3,3,3,3,
3,3,3,3,3,3,3,3,3,3,3,3,3,3,3,3,3,3,3,3,3,3,3,3,3,3,3,3,3,3,3,3,3,3,3,3,
3,3,3,3,3,3,3,3,3,3,3,3,3,3,3,3,3,3,3,3,3,3,4),(-10.3757270559041,-10.2869920871581,
-10.1977381029001,-10.108217706739,-10.0183574668925,-9.98983502199165,
-9.90986528326832,-9.82998988698337,-9.75019131838053,-9.67045212311163,
-9.59075489377989,-9.51107080616828,-9.43139017068793,-9.35169726874048,
-9.27197637739935,-9.19216798373438,-9.11231044011139,-9.03233927145686,
-8.99085151979248,-8.91090124579369,-8.8310453591876,-8.75126632648789,
-8.67154667478177,-8.59186897821204,-8.51220434532162,-8.4325431142785,
-8.35286954991441,-8.27316791267112,-8.19337854952507,-8.11353993816696,
-8.03358738564243,-7.99186801759332,-7.91189007011555,-7.83200655967694,
-7.75219997789339,-7.67245287681802,-7.59274785550133,-7.51305616936823,
-7.43336805599691,-7.3536678028127,-7.27393969299786,-7.19412431776395,
-7.1142599163916,-7.03428214115358,-6.99288451539415,-6.91289368398352,
-6.83299702701498,-6.75317705182906,-6.6734163258982,-6.59369746344528,
-6.51399165994175,-6.43428925966801,-6.35457456318493,-6.27483186672925,
-6.19500176270018,-6.1151225302351,-6.03512989349482,-5.99390101319498,
-5.91403497940862,-5.83426347376325,-5.75456888393364,-5.67493365889373,
-5.59534029512317,-5.51575959094961,-5.43618203185169,-5.35659181285564,
-5.27697312429453,-5.19726569154639,-5.11750855838175,-5.03763607409116,
-4.99491751099582,-4.9158035640275,-4.83678366946472,-4.7578395671856,-4.67895306886685,
-4.60010142097271,-4.52126630226961,-4.442431337671,-4.3635801545808,-4.28465880105462,
-4.20569728010626,-4.12663765514124,-4.0925417489438),.UNSPECIFIED.);
#310=B_SPLINE_CURVE_WITH_KNOTS('',3,(#24565,#24566,#24567,#24568,#24569,
#24570,#24571,#24572,#24573,#24574,#24575,#24576,#24577,#24578,#24579,#24580,
#24581,#24582,#24583,#24584,#24585,#24586,#24587,#24588,#24589,#24590,#24591,
#24592,#24593,#24594,#24595,#24596,#24597,#24598,#24599,#24600,#24601,#24602,
#24603,#24604,#24605,#24606,#24607,#24608,#24609,#24610,#24611,#24612,#24613),
 .UNSPECIFIED.,.F.,.F.,(4,3,3,3,3,3,3,3,3,3,3,3,3,3,3,3,4),(656.592864600441,
656.688389105084,656.784357962551,656.880910721209,656.958763939773,657.040980201405,
657.123093290724,657.205124599147,657.290121131882,657.372060131357,657.453986833998,
657.535920394155,657.617879970969,657.69992876607,657.782030759269,657.864248468546,
657.885096861028),.UNSPECIFIED.);
#311=B_SPLINE_CURVE_WITH_KNOTS('',3,(#24617,#24618,#24619,#24620,#24621,
#24622,#24623,#24624,#24625,#24626,#24627,#24628),.UNSPECIFIED.,.F.,.F.,
(4,2,2,2,2,4),(1.19797002426947E-5,0.013145050983649,0.0211198128453241,
0.0241087294059435,0.0252409894393879,0.0262779747017448),.UNSPECIFIED.);
#312=B_SPLINE_CURVE_WITH_KNOTS('',3,(#24630,#24631,#24632,#24633,#24634,
#24635,#24636,#24637,#24638,#24639,#24640,#24641,#24642,#24643,#24644,#24645,
#24646,#24647,#24648,#24649,#24650,#24651,#24652,#24653,#24654,#24655,#24656,
#24657,#24658,#24659,#24660,#24661,#24662,#24663,#24664,#24665,#24666,#24667,
#24668,#24669,#24670,#24671,#24672,#24673,#24674,#24675,#24676,#24677,#24678,
#24679,#24680,#24681,#24682,#24683,#24684,#24685,#24686,#24687,#24688,#24689,
#24690,#24691,#24692,#24693,#24694,#24695,#24696,#24697,#24698,#24699,#24700,
#24701,#24702,#24703,#24704,#24705,#24706,#24707,#24708,#24709,#24710,#24711,
#24712,#24713,#24714,#24715,#24716,#24717,#24718,#24719,#24720,#24721,#24722,
#24723,#24724,#24725,#24726,#24727,#24728,#24729,#24730,#24731,#24732,#24733,
#24734,#24735,#24736,#24737,#24738,#24739,#24740,#24741,#24742,#24743,#24744,
#24745,#24746,#24747,#24748,#24749,#24750,#24751,#24752,#24753,#24754,#24755,
#24756,#24757,#24758,#24759,#24760,#24761,#24762,#24763,#24764,#24765,#24766,
#24767,#24768,#24769,#24770,#24771,#24772,#24773,#24774,#24775,#24776,#24777,
#24778,#24779,#24780,#24781,#24782,#24783,#24784,#24785,#24786,#24787,#24788,
#24789,#24790,#24791,#24792,#24793,#24794,#24795,#24796,#24797,#24798,#24799,
#24800,#24801,#24802,#24803,#24804,#24805,#24806,#24807,#24808,#24809,#24810,
#24811,#24812,#24813,#24814,#24815,#24816,#24817,#24818,#24819,#24820,#24821,
#24822,#24823,#24824,#24825,#24826,#24827,#24828,#24829,#24830,#24831,#24832,
#24833,#24834,#24835,#24836,#24837,#24838,#24839,#24840,#24841,#24842,#24843,
#24844,#24845,#24846,#24847,#24848,#24849,#24850,#24851,#24852,#24853,#24854,
#24855),.UNSPECIFIED.,.F.,.F.,(4,3,3,3,3,3,3,3,3,3,3,3,3,3,3,3,3,3,3,3,
3,3,3,3,3,3,3,3,3,3,3,3,3,3,3,3,3,3,3,3,3,3,3,3,3,3,3,3,3,3,3,3,3,3,3,3,
3,3,3,3,3,3,3,3,3,3,3,3,3,3,3,3,3,3,3,4),(650.309679293274,650.406233622475,
650.503311876305,650.601029081094,650.652314781296,650.735957910548,650.819497813811,
650.902954720291,650.986348786315,651.069707913455,651.153049944518,651.236393038061,
651.319755349584,651.403207547017,651.486704935601,651.570337997441,651.651298283496,
651.735161305775,651.81892086122,651.902596957108,651.986209529205,652.069785368016,
652.153342989141,652.236900352737,652.320475414888,652.404136776,652.487841704887,
652.571677452732,652.650281785695,652.734167640835,652.817951928372,652.901654602967,
652.985295549612,653.068902358886,653.152492521882,653.236083957684,653.3196945823,
653.403393630556,653.487137462525,653.571013769074,653.649265287894,653.732279311988,
653.815189413488,653.898016396369,653.980780982524,654.06421445847,654.146931315586,
654.229651530997,654.312393764629,654.396357520995,654.479246476447,654.56374763327,
654.648248790093,654.733255939278,654.818152347384,654.902956529104,654.987686922183,
655.072360395319,655.157002738458,655.24163054438,655.326260392304,655.410945674027,
655.495658757372,655.580466457639,655.647232292292,655.731132100585,655.814963062839,
655.898744863005,655.982495865332,656.066255250149,656.146724043392,656.24281480375,
656.339248498341,656.43578222174,656.532319067256,656.592864600267),
 .UNSPECIFIED.);
#313=B_SPLINE_CURVE_WITH_KNOTS('',3,(#24857,#24858,#24859,#24860,#24861,
#24862,#24863,#24864,#24865,#24866,#24867,#24868,#24869,#24870,#24871,#24872,
#24873,#24874,#24875,#24876,#24877,#24878,#24879,#24880,#24881,#24882,#24883,
#24884,#24885,#24886,#24887,#24888,#24889,#24890,#24891,#24892,#24893,#24894,
#24895,#24896,#24897,#24898,#24899,#24900,#24901,#24902,#24903,#24904,#24905,
#24906,#24907,#24908,#24909,#24910,#24911,#24912,#24913,#24914,#24915,#24916,
#24917,#24918,#24919,#24920,#24921,#24922,#24923,#24924,#24925,#24926,#24927,
#24928,#24929,#24930,#24931,#24932,#24933,#24934,#24935,#24936,#24937,#24938,
#24939,#24940,#24941,#24942,#24943,#24944,#24945,#24946,#24947,#24948,#24949,
#24950,#24951,#24952,#24953,#24954,#24955,#24956,#24957,#24958,#24959,#24960,
#24961,#24962,#24963,#24964,#24965,#24966,#24967,#24968,#24969,#24970,#24971,
#24972,#24973,#24974,#24975,#24976,#24977,#24978,#24979,#24980,#24981,#24982,
#24983,#24984,#24985,#24986,#24987,#24988,#24989,#24990,#24991,#24992,#24993,
#24994,#24995,#24996,#24997,#24998,#24999,#25000,#25001,#25002,#25003,#25004,
#25005,#25006,#25007,#25008,#25009,#25010,#25011,#25012,#25013,#25014,#25015,
#25016,#25017,#25018,#25019,#25020,#25021,#25022,#25023,#25024,#25025,#25026,
#25027,#25028,#25029,#25030,#25031,#25032,#25033,#25034,#25035,#25036,#25037,
#25038,#25039,#25040,#25041,#25042,#25043,#25044,#25045,#25046,#25047,#25048,
#25049,#25050,#25051,#25052,#25053,#25054,#25055,#25056,#25057,#25058,#25059,
#25060,#25061,#25062,#25063,#25064,#25065,#25066,#25067,#25068,#25069,#25070,
#25071,#25072,#25073,#25074,#25075,#25076,#25077,#25078,#25079,#25080,#25081,
#25082,#25083,#25084,#25085),.UNSPECIFIED.,.F.,.F.,(4,3,3,3,3,3,3,3,3,3,
3,3,3,3,3,3,3,3,3,3,3,3,3,3,3,3,3,3,3,3,3,3,3,3,3,3,3,3,3,3,3,3,3,3,3,3,
3,3,3,3,3,3,3,3,3,3,3,3,3,3,3,3,3,3,3,3,3,3,3,3,3,3,3,3,3,3,4),(644.026493985908,
644.110429528115,644.194368280084,644.278327608105,644.362324888035,644.446429579001,
644.530594543763,644.614894173054,644.658413768101,644.742158268002,644.825799710795,
644.909358221521,644.992853853304,645.076314136271,645.159757062121,645.243200697321,
645.326663104971,645.410214134101,645.493809825012,645.577539290062,645.657397270301,
645.741145449423,645.824790560255,645.908352724234,645.991851990903,646.075315868383,
646.158762363715,646.242209540124,646.325675457446,646.409229926937,646.492829025913,
646.576561809727,646.6563807725,646.740132511195,646.823781225058,646.907347031259,
646.990849975135,647.074317569564,647.15776780545,647.241218742351,647.32468843645,
647.408246686763,647.491849574731,647.575586122846,647.655364274699,647.739095628126,
647.8227239079,647.906269252696,647.989751729165,648.073198918806,648.156628790793,
648.240059423682,648.323508892707,648.407047156379,648.490630155869,648.5743471839,
648.654347776898,648.738108112563,648.821765319466,648.905339507456,648.988850714513,
649.072326364678,649.155784529117,649.23924326054,649.322720608183,649.406286247826,
649.489896392915,649.573639900747,649.653331279097,649.737173540448,649.820914313398,
649.904571670437,649.988163622653,650.071711157331,650.155231024935,650.238761690986,
650.309679293087),.UNSPECIFIED.);
#314=B_SPLINE_CURVE_WITH_KNOTS('',3,(#25087,#25088,#25089,#25090,#25091,
#25092,#25093,#25094,#25095,#25096,#25097,#25098,#25099,#25100,#25101,#25102,
#25103,#25104,#25105,#25106,#25107,#25108,#25109,#25110,#25111,#25112,#25113,
#25114,#25115,#25116,#25117,#25118,#25119,#25120,#25121,#25122,#25123,#25124,
#25125,#25126,#25127,#25128,#25129,#25130,#25131,#25132,#25133,#25134,#25135,
#25136,#25137,#25138,#25139,#25140,#25141,#25142,#25143,#25144,#25145,#25146,
#25147,#25148,#25149,#25150,#25151,#25152,#25153,#25154,#25155,#25156,#25157,
#25158,#25159,#25160,#25161,#25162,#25163,#25164,#25165,#25166,#25167,#25168,
#25169,#25170,#25171,#25172,#25173,#25174,#25175,#25176,#25177,#25178,#25179,
#25180,#25181,#25182,#25183,#25184,#25185,#25186,#25187,#25188,#25189,#25190,
#25191,#25192,#25193,#25194,#25195,#25196,#25197,#25198,#25199,#25200,#25201,
#25202,#25203,#25204,#25205,#25206,#25207,#25208,#25209,#25210,#25211,#25212,
#25213,#25214,#25215,#25216,#25217,#25218,#25219,#25220,#25221,#25222,#25223,
#25224,#25225,#25226,#25227,#25228,#25229,#25230,#25231,#25232,#25233,#25234,
#25235,#25236,#25237,#25238,#25239,#25240,#25241,#25242,#25243,#25244,#25245,
#25246,#25247,#25248,#25249,#25250,#25251,#25252,#25253,#25254,#25255,#25256,
#25257,#25258,#25259,#25260,#25261,#25262,#25263,#25264,#25265,#25266,#25267,
#25268,#25269,#25270,#25271,#25272,#25273,#25274,#25275,#25276,#25277,#25278,
#25279,#25280,#25281,#25282,#25283,#25284,#25285,#25286,#25287,#25288,#25289,
#25290,#25291,#25292,#25293,#25294,#25295,#25296,#25297,#25298,#25299,#25300,
#25301,#25302,#25303,#25304,#25305,#25306,#25307,#25308,#25309,#25310,#25311,
#25312),.UNSPECIFIED.,.F.,.F.,(4,3,3,3,3,3,3,3,3,3,3,3,3,3,3,3,3,3,3,3,
3,3,3,3,3,3,3,3,3,3,3,3,3,3,3,3,3,3,3,3,3,3,3,3,3,3,3,3,3,3,3,3,3,3,3,3,
3,3,3,3,3,3,3,3,3,3,3,3,3,3,3,3,3,3,3,4),(637.743308678856,637.826129299476,
637.908853701098,637.991502818153,638.075629060247,638.158199624338,638.240762291769,
638.323335862189,638.408630085369,638.491326062699,638.577919408802,638.664512754906,
638.748259443697,638.831903076827,638.915463777078,638.998961595333,639.08242405252,
639.16586914484,639.249314936754,639.332779489347,639.416332632809,639.499930424729,
639.583661946882,639.663496257106,639.747242994695,639.830886676261,639.914447424539,
639.99794529037,640.081407794284,640.164852932809,640.248298770366,640.331763367998,
640.415316555299,640.498914390473,640.58264595445,640.662479759305,640.746226638579,
640.829870462765,640.913431354442,640.996929364293,641.080392012657,641.163837295875,
641.247283278227,641.330748020618,641.414301351801,641.497899330607,641.581631036332,
641.661463261504,641.745209677247,641.828853037284,641.912413464676,641.995911010585,
642.079373197151,642.162818019937,642.246263543652,642.329727829631,642.413280710478,
642.496878241542,642.580609508471,642.660446763703,642.744193621587,642.82783742169,
642.911398286652,642.994896267213,643.078358882516,643.161804130387,643.245250075151,
643.328714777759,643.412268065945,643.495865999938,643.57959765823,643.659430265902,
643.754828788849,643.849906489669,643.94436720848,644.026493985711),
 .UNSPECIFIED.);
#315=B_SPLINE_CURVE_WITH_KNOTS('',3,(#25314,#25315,#25316,#25317,#25318,
#25319,#25320,#25321,#25322,#25323,#25324,#25325,#25326,#25327,#25328,#25329,
#25330,#25331,#25332,#25333,#25334,#25335,#25336,#25337,#25338,#25339,#25340,
#25341,#25342,#25343,#25344,#25345,#25346,#25347,#25348,#25349,#25350,#25351,
#25352,#25353,#25354,#25355,#25356,#25357,#25358,#25359,#25360,#25361,#25362,
#25363,#25364,#25365,#25366,#25367,#25368,#25369,#25370,#25371,#25372,#25373,
#25374,#25375,#25376,#25377,#25378,#25379,#25380,#25381,#25382,#25383,#25384,
#25385,#25386,#25387,#25388,#25389,#25390,#25391,#25392,#25393,#25394,#25395,
#25396,#25397,#25398,#25399,#25400,#25401,#25402,#25403,#25404,#25405,#25406,
#25407,#25408,#25409,#25410,#25411,#25412,#25413,#25414,#25415,#25416,#25417,
#25418,#25419,#25420,#25421,#25422,#25423,#25424,#25425,#25426,#25427,#25428,
#25429,#25430,#25431,#25432,#25433,#25434,#25435,#25436,#25437,#25438,#25439,
#25440,#25441,#25442,#25443,#25444,#25445,#25446,#25447,#25448,#25449,#25450,
#25451,#25452,#25453,#25454,#25455,#25456,#25457,#25458,#25459,#25460,#25461,
#25462,#25463,#25464,#25465,#25466,#25467,#25468,#25469,#25470,#25471,#25472,
#25473,#25474,#25475,#25476,#25477,#25478,#25479,#25480,#25481,#25482,#25483,
#25484,#25485,#25486,#25487,#25488,#25489,#25490,#25491,#25492,#25493,#25494,
#25495,#25496,#25497,#25498,#25499,#25500,#25501,#25502,#25503,#25504,#25505,
#25506,#25507,#25508,#25509,#25510,#25511,#25512,#25513,#25514,#25515,#25516,
#25517,#25518,#25519,#25520,#25521,#25522,#25523,#25524,#25525,#25526,#25527,
#25528,#25529,#25530,#25531,#25532,#25533,#25534,#25535,#25536,#25537,#25538,
#25539),.UNSPECIFIED.,.F.,.F.,(4,3,3,3,3,3,3,3,3,3,3,3,3,3,3,3,3,3,3,3,
3,3,3,3,3,3,3,3,3,3,3,3,3,3,3,3,3,3,3,3,3,3,3,3,3,3,3,3,3,3,3,3,3,3,3,3,
3,3,3,3,3,3,3,3,3,3,3,3,3,3,3,3,3,3,3,4),(631.460123371549,631.576925539142,
631.671628239512,631.755374972795,631.839018650393,631.922579395042,632.006077257582,
632.089539758726,632.172984894798,632.256430730218,632.339895326032,632.423448512022,
632.50704634616,632.590777909577,632.670611741711,632.754358473643,632.83800214989,
632.921562893191,633.005060754385,633.088523254193,633.171968388935,633.255414223033,
633.338878817533,633.42243200223,633.506029835084,633.589761397246,633.669595243911,
633.753341976116,633.836985652626,633.920546396179,634.004044257616,634.08750675765,
634.170951892609,634.254397726913,634.337862321609,634.421415506485,634.505013339509,
634.588744901824,634.66857874611,634.752325482574,634.835969163363,634.919529911209,
635.003027776947,635.086490281281,635.169935420539,635.253381259137,635.336845858117,
635.420399047238,635.503996884493,635.587728450971,635.667562248309,635.751308975095,
635.834952646204,635.918513384376,636.002011240459,636.085473735198,636.168918864898,
636.252364693986,636.335829283511,636.419382463317,636.50298029132,636.586711848743,
636.666545750508,636.750292481885,636.833936157522,636.917496900159,637.000994760638,
637.084457259654,637.167902393558,637.251348226774,637.334812820347,637.418366004053,
637.501963835881,637.585695396965,637.665529252707,637.743308678728),
 .UNSPECIFIED.);
#316=B_SPLINE_CURVE_WITH_KNOTS('',3,(#25541,#25542,#25543,#25544,#25545,
#25546,#25547,#25548,#25549,#25550,#25551,#25552,#25553,#25554,#25555,#25556,
#25557,#25558,#25559,#25560,#25561,#25562,#25563,#25564,#25565,#25566,#25567,
#25568,#25569,#25570,#25571,#25572,#25573,#25574,#25575,#25576,#25577,#25578,
#25579,#25580,#25581,#25582,#25583,#25584,#25585,#25586,#25587,#25588,#25589,
#25590,#25591,#25592,#25593,#25594,#25595,#25596,#25597,#25598,#25599,#25600,
#25601,#25602,#25603,#25604,#25605,#25606,#25607,#25608,#25609,#25610,#25611,
#25612,#25613,#25614,#25615,#25616,#25617,#25618,#25619,#25620,#25621,#25622,
#25623,#25624,#25625,#25626,#25627,#25628,#25629,#25630,#25631,#25632,#25633,
#25634,#25635,#25636,#25637,#25638,#25639,#25640,#25641,#25642,#25643,#25644,
#25645,#25646,#25647,#25648,#25649,#25650,#25651,#25652,#25653,#25654,#25655,
#25656,#25657,#25658,#25659,#25660,#25661,#25662,#25663,#25664,#25665,#25666,
#25667,#25668,#25669,#25670,#25671,#25672,#25673,#25674,#25675,#25676,#25677,
#25678,#25679,#25680,#25681,#25682,#25683,#25684,#25685,#25686,#25687,#25688,
#25689,#25690,#25691,#25692,#25693,#25694,#25695,#25696,#25697,#25698,#25699,
#25700,#25701,#25702,#25703,#25704,#25705,#25706,#25707,#25708,#25709,#25710,
#25711,#25712,#25713,#25714,#25715,#25716,#25717,#25718,#25719,#25720,#25721,
#25722,#25723,#25724,#25725,#25726,#25727,#25728,#25729,#25730,#25731,#25732,
#25733,#25734,#25735,#25736,#25737,#25738,#25739,#25740,#25741,#25742,#25743,
#25744,#25745,#25746,#25747,#25748,#25749,#25750,#25751,#25752,#25753,#25754,
#25755,#25756,#25757,#25758,#25759,#25760,#25761,#25762,#25763,#25764,#25765,
#25766,#25767,#25768,#25769),.UNSPECIFIED.,.F.,.F.,(4,3,3,3,3,3,3,3,3,3,
3,3,3,3,3,3,3,3,3,3,3,3,3,3,3,3,3,3,3,3,3,3,3,3,3,3,3,3,3,3,3,3,3,3,3,3,
3,3,3,3,3,3,3,3,3,3,3,3,3,3,3,3,3,3,3,3,3,3,3,3,3,3,3,3,3,3,4),(625.176938064369,
625.264298823443,625.351772685274,625.439451113209,625.52723733009,625.615223939944,
625.677727226317,625.761473959032,625.845117636061,625.92867838014,626.01217624211,
626.095638742685,626.179083878191,626.262529713046,626.345994308297,626.429547493731,
626.513145327317,626.596876890191,626.676710728516,626.760457461207,626.844101138212,
626.927661882267,627.011159744213,627.094622244765,627.178067380246,627.261513215078,
627.344977810306,627.428530995718,627.51212882928,627.595860392133,627.675694230716,
627.759440963395,627.843084640387,627.92664538443,628.010143246363,628.093605746902,
628.17705088237,628.260496717189,628.343961312403,628.427514497801,628.51111233135,
628.594843894188,628.674677732915,628.758424465705,628.842068142808,628.925628886963,
629.009126749007,629.092589249658,629.176034385237,629.259480220167,629.342944815492,
629.426498000999,629.510095834656,629.593827397601,629.673661235114,629.75740796772,
629.84105164464,629.924612388612,630.008110250474,630.091572750943,630.175017886342,
630.258463721093,630.34192831624,630.425481501573,630.509079335057,630.592810897833,
630.672644737313,630.755224498922,630.837700764635,630.920082197797,631.00241054239,
631.084704824653,631.16698403934,631.249295852495,631.331625039562,631.414029479979,
631.460123371422),.UNSPECIFIED.);
#317=B_SPLINE_CURVE_WITH_KNOTS('',3,(#25771,#25772,#25773,#25774,#25775,
#25776,#25777,#25778,#25779,#25780,#25781,#25782,#25783,#25784,#25785,#25786,
#25787,#25788,#25789,#25790,#25791,#25792,#25793,#25794,#25795,#25796,#25797,
#25798,#25799,#25800,#25801,#25802,#25803,#25804,#25805,#25806,#25807,#25808,
#25809,#25810,#25811,#25812,#25813,#25814,#25815,#25816,#25817,#25818,#25819,
#25820,#25821,#25822,#25823,#25824,#25825,#25826,#25827,#25828,#25829,#25830,
#25831,#25832,#25833,#25834,#25835,#25836,#25837,#25838,#25839,#25840,#25841,
#25842,#25843,#25844,#25845,#25846,#25847,#25848,#25849,#25850,#25851,#25852,
#25853,#25854,#25855,#25856,#25857,#25858,#25859,#25860,#25861,#25862,#25863,
#25864,#25865,#25866,#25867,#25868,#25869,#25870,#25871,#25872,#25873,#25874,
#25875,#25876,#25877,#25878,#25879,#25880,#25881,#25882,#25883,#25884,#25885,
#25886,#25887,#25888,#25889,#25890,#25891,#25892,#25893,#25894,#25895,#25896,
#25897,#25898,#25899,#25900,#25901,#25902,#25903,#25904,#25905,#25906,#25907,
#25908,#25909,#25910,#25911,#25912,#25913,#25914,#25915,#25916,#25917,#25918,
#25919,#25920,#25921,#25922,#25923,#25924,#25925,#25926,#25927,#25928,#25929,
#25930,#25931,#25932,#25933,#25934,#25935,#25936,#25937,#25938,#25939,#25940,
#25941,#25942,#25943,#25944,#25945,#25946,#25947,#25948,#25949,#25950,#25951,
#25952,#25953,#25954,#25955,#25956,#25957,#25958,#25959,#25960,#25961,#25962,
#25963,#25964,#25965,#25966,#25967,#25968,#25969,#25970,#25971,#25972,#25973,
#25974,#25975,#25976,#25977,#25978,#25979,#25980,#25981,#25982,#25983,#25984,
#25985,#25986,#25987,#25988,#25989,#25990,#25991,#25992,#25993,#25994,#25995,
#25996,#25997,#25998,#25999),.UNSPECIFIED.,.F.,.F.,(4,3,3,3,3,3,3,3,3,3,
3,3,3,3,3,3,3,3,3,3,3,3,3,3,3,3,3,3,3,3,3,3,3,3,3,3,3,3,3,3,3,3,3,3,3,3,
3,3,3,3,3,3,3,3,3,3,3,3,3,3,3,3,3,3,3,3,3,3,3,3,3,3,3,3,3,3,4),(618.893752757332,
618.976157287315,619.058495611027,619.140795072643,619.223076019747,619.305357440849,
619.387658322558,619.47004462904,619.552477968653,619.63503337098,619.683826213122,
619.767572945824,619.851216622841,619.934777366907,620.018275228864,620.101737729427,
620.18518286492,620.268628699763,620.352093295002,620.435646480424,620.519244313997,
620.602975876859,620.682809715321,620.766556448023,620.850200125039,620.933760869105,
621.017258731062,621.100721231624,621.184166367117,621.267612201959,621.351076797197,
621.434629982619,621.518227816192,621.601959379054,621.681793217521,621.765539950222,
621.849183627237,621.932744371303,622.016242233259,622.099704733821,622.183149869312,
622.266595704154,622.350060299391,622.433613484812,622.517211318384,622.600942881245,
622.68077671972,622.764523452424,622.848167129442,622.93172787351,623.015225735468,
623.098688236033,623.182133371527,623.265579206372,623.349043801612,623.432596987036,
623.51619482061,623.599926383474,623.679760221919,623.76350695462,623.847150631634,
623.930711375699,624.014209237655,624.097671738216,624.181116873707,624.264562708549,
624.348027303786,624.431580489207,624.515178322779,624.59890988564,624.678743724118,
624.766852498131,624.854808775082,624.942563062619,625.030197091654,625.117672902589,
625.176938064065),.UNSPECIFIED.);
#318=B_SPLINE_CURVE_WITH_KNOTS('',3,(#26001,#26002,#26003,#26004,#26005,
#26006,#26007,#26008,#26009,#26010,#26011,#26012,#26013,#26014,#26015,#26016,
#26017,#26018,#26019,#26020,#26021,#26022,#26023,#26024,#26025,#26026,#26027,
#26028,#26029,#26030,#26031,#26032,#26033,#26034,#26035,#26036,#26037,#26038,
#26039,#26040,#26041,#26042,#26043,#26044,#26045,#26046,#26047,#26048,#26049,
#26050,#26051,#26052,#26053,#26054,#26055,#26056,#26057,#26058,#26059,#26060,
#26061,#26062,#26063,#26064,#26065,#26066,#26067,#26068,#26069,#26070,#26071,
#26072,#26073,#26074,#26075,#26076,#26077,#26078,#26079,#26080,#26081,#26082,
#26083,#26084,#26085,#26086,#26087,#26088,#26089,#26090,#26091,#26092,#26093,
#26094,#26095,#26096,#26097,#26098,#26099,#26100,#26101,#26102,#26103,#26104,
#26105,#26106,#26107,#26108,#26109,#26110,#26111,#26112,#26113,#26114,#26115,
#26116,#26117,#26118,#26119,#26120,#26121,#26122,#26123,#26124,#26125,#26126,
#26127,#26128,#26129,#26130,#26131,#26132,#26133,#26134,#26135,#26136,#26137,
#26138,#26139,#26140,#26141,#26142,#26143,#26144,#26145,#26146,#26147,#26148,
#26149,#26150,#26151,#26152,#26153,#26154,#26155,#26156,#26157,#26158,#26159,
#26160,#26161,#26162,#26163,#26164,#26165,#26166,#26167,#26168,#26169,#26170,
#26171,#26172,#26173,#26174,#26175,#26176,#26177,#26178,#26179,#26180,#26181,
#26182,#26183,#26184,#26185,#26186,#26187,#26188,#26189,#26190,#26191,#26192,
#26193,#26194,#26195,#26196,#26197,#26198,#26199,#26200,#26201,#26202,#26203,
#26204,#26205,#26206,#26207,#26208,#26209,#26210,#26211,#26212,#26213,#26214,
#26215,#26216,#26217,#26218,#26219,#26220,#26221,#26222,#26223,#26224,#26225,
#26226),.UNSPECIFIED.,.F.,.F.,(4,3,3,3,3,3,3,3,3,3,3,3,3,3,3,3,3,3,3,3,
3,3,3,3,3,3,3,3,3,3,3,3,3,3,3,3,3,3,3,3,3,3,3,3,3,3,3,3,3,3,3,3,3,3,3,3,
3,3,3,3,3,3,3,3,3,3,3,3,3,3,3,3,3,3,3,4),(612.61056745001,612.690941697728,
612.77468843043,612.858332107446,612.941892851513,613.02539071347,613.108853214032,
613.192298349525,613.275744184368,613.359208779606,613.442761965028,613.5263597986,
613.610091361462,613.689925199927,613.773671932629,613.857315609645,613.940876353711,
614.024374215668,614.10783671623,614.191281851722,614.274727686565,614.358192281803,
614.441745467225,614.525343300797,614.609074863659,614.688908702126,614.772655434828,
614.856299111844,614.939859855911,615.023357717868,615.10682021843,615.190265353923,
615.273711188766,615.357175784004,615.440728969426,615.524326802999,615.608058365861,
615.687892204326,615.771638937028,615.855282614044,615.938843358111,616.022341220067,
616.10580372063,616.189248856123,616.272694690965,616.356159286204,616.439712471626,
616.523310305198,616.60704186806,616.686875706525,616.770622439227,616.854266116243,
616.937826860309,617.021324722265,617.104787222828,617.18823235832,617.271678193163,
617.355142788401,617.438695973823,617.522293807395,617.606025370257,617.685859208724,
617.769605941426,617.853249618442,617.936810362508,618.020308224465,618.103770725028,
618.18721586052,618.270661695363,618.354126290601,618.437679476023,618.521277309595,
618.605008872457,618.684842710923,618.802340309998,618.893752757189),
 .UNSPECIFIED.);
#319=B_SPLINE_CURVE_WITH_KNOTS('',3,(#26228,#26229,#26230,#26231,#26232,
#26233,#26234,#26235,#26236,#26237,#26238,#26239,#26240,#26241,#26242,#26243,
#26244,#26245,#26246,#26247,#26248,#26249,#26250,#26251,#26252,#26253,#26254,
#26255,#26256,#26257,#26258,#26259,#26260,#26261,#26262,#26263,#26264,#26265,
#26266,#26267,#26268,#26269,#26270,#26271,#26272,#26273,#26274,#26275,#26276,
#26277,#26278,#26279,#26280,#26281,#26282,#26283,#26284,#26285,#26286,#26287,
#26288,#26289,#26290,#26291,#26292,#26293,#26294,#26295,#26296,#26297,#26298,
#26299,#26300,#26301,#26302,#26303,#26304,#26305,#26306,#26307,#26308,#26309,
#26310,#26311,#26312,#26313,#26314,#26315,#26316,#26317,#26318,#26319,#26320,
#26321,#26322,#26323,#26324,#26325,#26326,#26327,#26328,#26329,#26330,#26331,
#26332,#26333,#26334,#26335,#26336,#26337,#26338,#26339,#26340,#26341,#26342,
#26343,#26344,#26345,#26346,#26347,#26348,#26349,#26350,#26351,#26352,#26353,
#26354,#26355,#26356,#26357,#26358,#26359,#26360,#26361,#26362,#26363,#26364,
#26365,#26366,#26367,#26368,#26369,#26370,#26371,#26372,#26373,#26374,#26375,
#26376,#26377,#26378,#26379,#26380,#26381,#26382,#26383,#26384,#26385,#26386,
#26387,#26388,#26389,#26390,#26391,#26392,#26393,#26394,#26395,#26396,#26397,
#26398,#26399,#26400,#26401,#26402,#26403,#26404,#26405,#26406,#26407,#26408,
#26409,#26410,#26411,#26412,#26413,#26414,#26415,#26416,#26417,#26418,#26419,
#26420,#26421,#26422,#26423,#26424,#26425,#26426,#26427,#26428,#26429,#26430,
#26431,#26432,#26433,#26434,#26435,#26436,#26437,#26438,#26439,#26440,#26441,
#26442,#26443,#26444,#26445,#26446,#26447,#26448,#26449,#26450,#26451,#26452,
#26453),.UNSPECIFIED.,.F.,.F.,(4,3,3,3,3,3,3,3,3,3,3,3,3,3,3,3,3,3,3,3,
3,3,3,3,3,3,3,3,3,3,3,3,3,3,3,3,3,3,3,3,3,3,3,3,3,3,3,3,3,3,3,3,3,3,3,3,
3,3,3,3,3,3,3,3,3,3,3,3,3,3,3,3,3,3,3,4),(606.32738214283,606.42167540976,
606.516348323315,606.611552029141,606.697040684533,606.780787417234,606.86443109425,
606.947991838316,607.031489700272,607.114952200834,607.198397336326,607.281843171168,
607.365307766405,607.448860951827,607.532458785399,607.61619034826,607.696024186732,
607.779770919434,607.86341459645,607.946975340516,608.030473202473,608.113935703035,
608.197380838527,608.28082667337,608.364291268608,608.44784445403,608.531442287603,
608.615173850464,608.695007688931,608.778754421633,608.86239809865,608.945958842717,
609.029456704674,609.112919205237,609.196364340729,609.279810175573,609.363274770811,
609.446827956234,609.530425789806,609.614157352669,609.693991191131,609.777737923833,
609.861381600849,609.944942344915,610.028440206872,610.111902707434,610.195347842926,
610.278793677769,610.362258273007,610.445811458429,610.529409292001,610.613140854863,
610.69297469333,610.776721426032,610.860365103047,610.943925847114,611.02742370907,
611.110886209633,611.194331345125,611.277777179968,611.361241775205,611.444794960627,
611.528392794199,611.612124357061,611.691958195529,611.774790308619,611.857520078192,
611.940168482096,612.023968353069,612.106523168124,612.189064409159,612.271610890298,
612.356350030193,612.439004220829,612.524785835355,612.61056744988),
 .UNSPECIFIED.);
#320=B_SPLINE_CURVE_WITH_KNOTS('',3,(#26455,#26456,#26457,#26458,#26459,
#26460,#26461,#26462,#26463,#26464),.UNSPECIFIED.,.F.,.F.,(4,1,1,1,1,1,
1,4),(600.044196835651,600.703139671338,601.702123173537,602.701106675736,
603.700090177936,604.699073680135,605.698057182334,606.32738214283),
 .UNSPECIFIED.);
#321=B_SPLINE_CURVE_WITH_KNOTS('',3,(#26466,#26467,#26468,#26469,#26470,
#26471,#26472,#26473,#26474,#26475,#26476,#26477,#26478,#26479,#26480,#26481,
#26482,#26483,#26484,#26485,#26486,#26487,#26488,#26489,#26490,#26491,#26492,
#26493,#26494,#26495,#26496,#26497,#26498,#26499,#26500,#26501,#26502,#26503,
#26504,#26505,#26506,#26507,#26508,#26509,#26510,#26511,#26512,#26513,#26514,
#26515,#26516,#26517,#26518,#26519,#26520,#26521,#26522,#26523,#26524,#26525,
#26526,#26527,#26528,#26529,#26530,#26531,#26532,#26533,#26534,#26535,#26536,
#26537,#26538,#26539,#26540,#26541,#26542,#26543,#26544,#26545,#26546,#26547,
#26548,#26549,#26550,#26551,#26552,#26553,#26554,#26555,#26556,#26557,#26558,
#26559,#26560,#26561,#26562,#26563,#26564,#26565,#26566,#26567,#26568,#26569,
#26570,#26571,#26572,#26573,#26574,#26575,#26576,#26577,#26578,#26579,#26580,
#26581,#26582,#26583,#26584,#26585,#26586,#26587,#26588,#26589,#26590,#26591,
#26592,#26593,#26594,#26595,#26596,#26597,#26598,#26599,#26600,#26601,#26602,
#26603,#26604,#26605,#26606,#26607,#26608,#26609,#26610,#26611,#26612,#26613,
#26614,#26615,#26616,#26617,#26618,#26619,#26620,#26621,#26622,#26623,#26624,
#26625,#26626,#26627,#26628,#26629,#26630,#26631,#26632,#26633,#26634,#26635,
#26636,#26637,#26638,#26639,#26640,#26641,#26642,#26643,#26644,#26645,#26646,
#26647,#26648,#26649,#26650,#26651,#26652,#26653,#26654,#26655,#26656,#26657,
#26658,#26659,#26660,#26661,#26662,#26663,#26664,#26665,#26666,#26667,#26668,
#26669,#26670,#26671,#26672,#26673,#26674,#26675,#26676,#26677,#26678,#26679,
#26680,#26681,#26682,#26683,#26684,#26685,#26686,#26687,#26688,#26689,#26690,
#26691,#26692,#26693,#26694),.UNSPECIFIED.,.F.,.F.,(4,3,3,3,3,3,3,3,3,3,
3,3,3,3,3,3,3,3,3,3,3,3,3,3,3,3,3,3,3,3,3,3,3,3,3,3,3,3,3,3,3,3,3,3,3,3,
3,3,3,3,3,3,3,3,3,3,3,3,3,3,3,3,3,3,3,3,3,3,3,3,3,3,3,3,3,3,4),(593.761011528671,
593.844095681974,593.927080015812,594.009985274574,594.092832125752,594.175649970121,
594.258455628379,594.341267723089,594.424104878142,594.507031806383,594.590010108476,
594.673108607956,594.709238658143,594.792985390845,594.876629067861,594.960189811927,
595.043687673884,595.127150174446,595.210595309938,595.294041144781,595.377505740019,
595.461058925441,595.544656759013,595.628388321875,595.708222160342,595.791968893044,
595.87561257006,595.959173314127,596.042671176084,596.126133676646,596.209578812139,
596.293024646982,596.37648924222,596.460042427641,596.543640261214,596.627371824076,
596.707205662541,596.790952395243,596.874596072259,596.958156816326,597.041654678282,
597.125117178845,597.208562314338,597.29200814918,597.375472744418,597.45902592984,
597.542623763413,597.626355326275,597.706189164741,597.789935897443,597.873579574459,
597.957140318525,598.040638180482,598.124100681045,598.207545816537,598.29099165138,
598.374456246618,598.45800943204,598.541607265612,598.625338828474,598.70517266694,
598.788919399642,598.872563076658,598.956123820724,599.03962168268,599.123084183243,
599.206529318735,599.289975153578,599.373439748816,599.456992934238,599.54059076781,
599.624322330672,599.704156169139,599.801883478083,599.89918974496,599.995709704988,
600.044196835651),.UNSPECIFIED.);
#322=B_SPLINE_CURVE_WITH_KNOTS('',3,(#26696,#26697,#26698,#26699,#26700,
#26701,#26702,#26703,#26704,#26705,#26706,#26707,#26708,#26709,#26710,#26711,
#26712,#26713,#26714,#26715,#26716,#26717,#26718,#26719,#26720,#26721,#26722,
#26723,#26724,#26725,#26726,#26727,#26728,#26729,#26730,#26731,#26732,#26733,
#26734,#26735,#26736,#26737,#26738,#26739,#26740,#26741,#26742,#26743,#26744,
#26745,#26746,#26747,#26748,#26749,#26750,#26751,#26752,#26753,#26754,#26755,
#26756,#26757,#26758,#26759,#26760,#26761,#26762,#26763,#26764,#26765,#26766,
#26767,#26768,#26769,#26770,#26771,#26772,#26773,#26774,#26775,#26776,#26777,
#26778,#26779,#26780,#26781,#26782,#26783,#26784,#26785,#26786,#26787,#26788,
#26789,#26790,#26791,#26792,#26793,#26794,#26795,#26796,#26797,#26798,#26799,
#26800,#26801,#26802,#26803,#26804,#26805,#26806,#26807,#26808,#26809,#26810,
#26811,#26812,#26813,#26814,#26815,#26816,#26817,#26818,#26819,#26820,#26821,
#26822,#26823,#26824,#26825,#26826,#26827,#26828,#26829,#26830,#26831,#26832,
#26833,#26834,#26835,#26836,#26837,#26838,#26839,#26840,#26841,#26842,#26843,
#26844,#26845,#26846,#26847,#26848,#26849,#26850,#26851,#26852,#26853,#26854,
#26855,#26856,#26857,#26858,#26859,#26860,#26861,#26862,#26863,#26864,#26865,
#26866,#26867,#26868,#26869,#26870,#26871,#26872,#26873,#26874,#26875,#26876,
#26877,#26878,#26879,#26880,#26881,#26882,#26883,#26884,#26885,#26886,#26887,
#26888,#26889,#26890,#26891,#26892,#26893,#26894,#26895,#26896,#26897,#26898,
#26899,#26900,#26901,#26902,#26903,#26904,#26905,#26906,#26907,#26908,#26909,
#26910,#26911,#26912,#26913,#26914,#26915,#26916,#26917,#26918,#26919,#26920,
#26921,#26922,#26923,#26924),.UNSPECIFIED.,.F.,.F.,(4,3,3,3,3,3,3,3,3,3,
3,3,3,3,3,3,3,3,3,3,3,3,3,3,3,3,3,3,3,3,3,3,3,3,3,3,3,3,3,3,3,3,3,3,3,3,
3,3,3,3,3,3,3,3,3,3,3,3,3,3,3,3,3,3,3,3,3,3,3,3,3,3,3,3,3,3,4),(587.477826221416,
587.58694029442,587.698877318794,587.716354142749,587.800100875451,587.883744552467,
587.967305296533,588.05080315849,588.134265659052,588.217710794545,588.301156629387,
588.384621224626,588.468174410047,588.55177224362,588.635503806482,588.715337644948,
588.79908437765,588.882728054666,588.966288798732,589.049786660689,589.133249161251,
589.216694296744,589.300140131586,589.383604726824,589.467157912246,589.550755745819,
589.634487308681,589.714321147147,589.798067879849,589.881711556865,589.965272300931,
590.048770162888,590.132232663451,590.215677798943,590.299123633786,590.382588229024,
590.466141414446,590.549739248018,590.63347081088,590.713304649346,590.797051382048,
590.880695059064,590.964255803131,591.047753665087,591.13121616565,591.214661301142,
591.298107135985,591.381571731223,591.465124916645,591.548722750218,591.63245431308,
591.712288151546,591.796034884248,591.879678561264,591.96323930533,592.046737167287,
592.13019966785,592.213644803342,592.297090638185,592.380555233423,592.464108418845,
592.547706252418,592.631437815279,592.711271653745,592.795018386447,592.878662063463,
592.962222807529,593.045720669486,593.129183170049,593.212628305541,593.296074140384,
593.379538735622,593.463091921044,593.546689754616,593.630421317478,593.710255155944,
593.761011528471),.UNSPECIFIED.);
#323=B_SPLINE_CURVE_WITH_KNOTS('',3,(#26926,#26927,#26928,#26929,#26930,
#26931,#26932,#26933,#26934,#26935,#26936,#26937,#26938,#26939,#26940,#26941,
#26942,#26943,#26944,#26945,#26946,#26947,#26948,#26949,#26950,#26951,#26952,
#26953,#26954,#26955,#26956,#26957,#26958,#26959,#26960,#26961,#26962,#26963,
#26964,#26965,#26966,#26967,#26968,#26969,#26970,#26971,#26972,#26973,#26974,
#26975,#26976,#26977,#26978,#26979,#26980,#26981,#26982,#26983,#26984,#26985,
#26986,#26987,#26988,#26989,#26990,#26991,#26992,#26993,#26994,#26995,#26996,
#26997,#26998,#26999,#27000,#27001,#27002,#27003,#27004,#27005,#27006,#27007,
#27008,#27009,#27010,#27011,#27012,#27013,#27014,#27015,#27016,#27017,#27018,
#27019,#27020,#27021,#27022,#27023,#27024,#27025,#27026,#27027,#27028,#27029,
#27030,#27031,#27032,#27033,#27034,#27035,#27036,#27037,#27038,#27039,#27040,
#27041,#27042,#27043,#27044,#27045,#27046,#27047,#27048,#27049,#27050,#27051,
#27052,#27053,#27054,#27055,#27056,#27057,#27058,#27059,#27060,#27061,#27062,
#27063,#27064,#27065,#27066,#27067,#27068,#27069,#27070,#27071,#27072,#27073,
#27074,#27075,#27076,#27077,#27078,#27079,#27080,#27081,#27082,#27083,#27084,
#27085,#27086,#27087,#27088,#27089,#27090,#27091,#27092,#27093,#27094,#27095,
#27096,#27097,#27098,#27099,#27100,#27101,#27102,#27103,#27104,#27105,#27106,
#27107,#27108,#27109,#27110,#27111,#27112,#27113,#27114,#27115,#27116,#27117,
#27118,#27119,#27120,#27121,#27122,#27123,#27124,#27125,#27126,#27127,#27128,
#27129,#27130,#27131,#27132,#27133,#27134,#27135,#27136,#27137,#27138,#27139,
#27140,#27141,#27142,#27143,#27144,#27145,#27146,#27147,#27148,#27149,#27150,
#27151,#27152,#27153,#27154),.UNSPECIFIED.,.F.,.F.,(4,3,3,3,3,3,3,3,3,3,
3,3,3,3,3,3,3,3,3,3,3,3,3,3,3,3,3,3,3,3,3,3,3,3,3,3,3,3,3,3,3,3,3,3,3,3,
3,3,3,3,3,3,3,3,3,3,3,3,3,3,3,3,3,3,3,3,3,3,3,3,3,3,3,3,3,3,4),(581.194640914112,
581.281091694881,581.367623639591,581.456331012082,581.543124164076,581.632788646815,
581.722453129554,581.806199862256,581.889843539272,581.973404283339,582.056902145296,
582.140364645859,582.223809781352,582.307255616195,582.390720211433,582.474273396855,
582.557871230428,582.64160279329,582.721436631753,582.805183364455,582.888827041471,
582.972387785537,583.055885647494,583.139348148056,583.222793283549,583.306239118392,
583.38970371363,583.473256899052,583.556854732624,583.640586295486,583.720420133952,
583.804166866654,583.887810543669,583.971371287735,584.054869149691,584.138331650253,
584.221776785745,584.305222620588,584.388687215826,584.472240401247,584.55583823482,
584.639569797681,584.719403636151,584.803150368853,584.886794045869,584.970354789936,
585.053852651893,585.137315152456,585.220760287949,585.304206122792,585.38767071803,
585.471223903452,585.554821737025,585.638553299887,585.718387138351,585.802133871053,
585.885777548069,585.969338292136,586.052836154092,586.136298654655,586.219743790147,
586.30318962499,586.386654220228,586.47020740565,586.553805239222,586.637536802084,
586.71737064055,586.800085950562,586.884803484403,586.967315565623,587.049773693441,
587.132196809623,587.21860416254,587.301037458573,587.383488199913,587.465999582898,
587.477826221292),.UNSPECIFIED.);
#324=B_SPLINE_CURVE_WITH_KNOTS('',3,(#27156,#27157,#27158,#27159,#27160,
#27161,#27162,#27163,#27164,#27165,#27166,#27167,#27168,#27169,#27170,#27171,
#27172,#27173,#27174,#27175,#27176,#27177,#27178,#27179,#27180,#27181,#27182,
#27183,#27184,#27185,#27186,#27187,#27188,#27189,#27190,#27191,#27192,#27193,
#27194,#27195,#27196,#27197,#27198,#27199,#27200,#27201,#27202,#27203,#27204,
#27205,#27206,#27207,#27208,#27209,#27210,#27211,#27212,#27213,#27214,#27215,
#27216,#27217,#27218,#27219,#27220,#27221,#27222,#27223,#27224,#27225,#27226,
#27227,#27228,#27229,#27230,#27231,#27232,#27233,#27234,#27235,#27236,#27237,
#27238,#27239,#27240,#27241,#27242,#27243,#27244,#27245,#27246,#27247,#27248,
#27249,#27250,#27251,#27252,#27253,#27254,#27255,#27256,#27257,#27258,#27259,
#27260,#27261,#27262,#27263,#27264,#27265,#27266,#27267,#27268,#27269,#27270,
#27271,#27272,#27273,#27274,#27275,#27276,#27277,#27278,#27279,#27280,#27281,
#27282,#27283,#27284,#27285,#27286,#27287,#27288,#27289,#27290,#27291,#27292,
#27293,#27294,#27295,#27296,#27297,#27298,#27299,#27300,#27301,#27302,#27303,
#27304,#27305,#27306,#27307,#27308,#27309,#27310,#27311,#27312,#27313,#27314,
#27315,#27316,#27317,#27318,#27319,#27320,#27321,#27322,#27323,#27324,#27325,
#27326,#27327,#27328,#27329,#27330,#27331,#27332,#27333,#27334,#27335,#27336,
#27337,#27338,#27339,#27340,#27341,#27342,#27343,#27344,#27345,#27346,#27347,
#27348,#27349,#27350,#27351,#27352,#27353,#27354,#27355,#27356,#27357,#27358,
#27359,#27360,#27361,#27362,#27363,#27364,#27365,#27366,#27367,#27368,#27369,
#27370,#27371,#27372,#27373,#27374,#27375,#27376,#27377,#27378,#27379,#27380,
#27381,#27382,#27383,#27384),.UNSPECIFIED.,.F.,.F.,(4,3,3,3,3,3,3,3,3,3,
3,3,3,3,3,3,3,3,3,3,3,3,3,3,3,3,3,3,3,3,3,3,3,3,3,3,3,3,3,3,3,3,3,3,3,3,
3,3,3,3,3,3,3,3,3,3,3,3,3,3,3,3,3,3,3,3,3,3,3,3,3,3,3,3,3,3,4),(574.911455607082,
574.993828450003,575.076127396377,575.158377281039,575.240601792619,575.322819962021,
575.40505081275,575.487363270994,575.569716742042,575.652199607108,575.728552116359,
575.812298849061,575.895942526077,575.979503270143,576.0630011321,576.146463632662,
576.229908768155,576.313354602997,576.396819198235,576.480372383657,576.56397021723,
576.647701780092,576.727535618558,576.81128235126,576.894926028276,576.978486772342,
577.061984634299,577.145447134861,577.228892270353,577.312338105196,577.395802700435,
577.479355885856,577.562953719429,577.64668528229,577.726519120757,577.810265853459,
577.893909530475,577.977470274541,578.060968136498,578.144430637061,578.227875772553,
578.311321607396,578.394786202633,578.478339388055,578.561937221628,578.64566878449,
578.725502622956,578.809249355658,578.892893032674,578.976453776741,579.059951638698,
579.143414139261,579.226859274753,579.310305109596,579.393769704834,579.477322890256,
579.560920723829,579.644652286691,579.724486125156,579.808232857858,579.891876534874,
579.97543727894,580.058935140897,580.14239764146,580.225842776952,580.309288611795,
580.392753207033,580.476306392455,580.559904226027,580.643635788889,580.723469627355,
580.812727000859,580.901812324686,580.990660382827,581.079361847327,581.167867105857,
581.194640913983),.UNSPECIFIED.);
#325=B_SPLINE_CURVE_WITH_KNOTS('',3,(#27386,#27387,#27388,#27389,#27390,
#27391,#27392,#27393,#27394,#27395,#27396,#27397,#27398,#27399,#27400,#27401,
#27402,#27403,#27404,#27405,#27406,#27407,#27408,#27409,#27410,#27411,#27412,
#27413,#27414,#27415,#27416,#27417,#27418,#27419,#27420,#27421,#27422,#27423,
#27424,#27425,#27426,#27427,#27428,#27429,#27430,#27431,#27432,#27433,#27434,
#27435,#27436,#27437,#27438,#27439,#27440,#27441,#27442,#27443,#27444,#27445,
#27446,#27447,#27448,#27449,#27450,#27451,#27452,#27453,#27454,#27455,#27456,
#27457,#27458,#27459,#27460,#27461,#27462,#27463,#27464,#27465,#27466,#27467,
#27468,#27469,#27470,#27471,#27472,#27473,#27474,#27475,#27476,#27477,#27478,
#27479,#27480,#27481,#27482,#27483,#27484,#27485,#27486,#27487,#27488,#27489,
#27490,#27491,#27492,#27493,#27494,#27495,#27496,#27497,#27498,#27499,#27500,
#27501,#27502,#27503,#27504,#27505,#27506,#27507,#27508,#27509,#27510,#27511,
#27512,#27513,#27514,#27515,#27516,#27517,#27518,#27519,#27520,#27521,#27522,
#27523,#27524,#27525,#27526,#27527,#27528,#27529,#27530,#27531,#27532,#27533,
#27534,#27535,#27536,#27537,#27538,#27539,#27540,#27541,#27542,#27543,#27544,
#27545,#27546,#27547,#27548,#27549,#27550,#27551,#27552,#27553,#27554,#27555,
#27556,#27557,#27558,#27559,#27560,#27561,#27562,#27563,#27564,#27565,#27566,
#27567,#27568,#27569,#27570,#27571,#27572,#27573,#27574,#27575,#27576,#27577,
#27578,#27579,#27580,#27581,#27582,#27583,#27584,#27585,#27586,#27587,#27588,
#27589,#27590,#27591,#27592,#27593,#27594,#27595,#27596,#27597,#27598,#27599,
#27600,#27601,#27602,#27603,#27604,#27605,#27606,#27607,#27608,#27609,#27610,
#27611),.UNSPECIFIED.,.F.,.F.,(4,3,3,3,3,3,3,3,3,3,3,3,3,3,3,3,3,3,3,3,
3,3,3,3,3,3,3,3,3,3,3,3,3,3,3,3,3,3,3,3,3,3,3,3,3,3,3,3,3,3,3,3,3,3,3,3,
3,3,3,3,3,3,3,3,3,3,3,3,3,3,3,3,3,3,3,4),(568.628270299753,568.735667600965,
568.819414333667,568.903058010683,568.986618754749,569.070116616706,569.153579117268,
569.23702425276,569.320470087603,569.403934682841,569.487487868263,569.571085701836,
569.654817264697,569.734651103164,569.818397835866,569.902041512882,569.985602256948,
570.069100118905,570.152562619467,570.23600775496,570.319453589802,570.402918185041,
570.486471370462,570.570069204035,570.653800766897,570.733634605363,570.817381338065,
570.901025015081,570.984585759148,571.068083621104,571.151546121667,571.234991257159,
571.318437092002,571.40190168724,571.485454872662,571.569052706235,571.652784269097,
571.732618107562,571.816364840264,571.90000851728,571.983569261346,572.067067123303,
572.150529623865,572.233974759358,572.3174205942,572.400885189439,572.48443837486,
572.568036208433,572.651767771295,572.731601609761,572.815348342463,572.898992019479,
572.982552763546,573.066050625502,573.149513126065,573.232958261557,573.3164040964,
573.399868691639,573.48342187706,573.567019710633,573.650751273495,573.730585111961,
573.814331844663,573.897975521679,573.981536265745,574.065034127702,574.148496628265,
574.231941763757,574.3153875986,574.398852193838,574.48240537926,574.566003212833,
574.649734775695,574.72956861416,574.855844314663,574.911455606932),
 .UNSPECIFIED.);
#326=B_SPLINE_CURVE_WITH_KNOTS('',3,(#27613,#27614,#27615,#27616,#27617,
#27618,#27619,#27620,#27621,#27622,#27623,#27624,#27625,#27626,#27627,#27628,
#27629,#27630,#27631,#27632,#27633,#27634,#27635,#27636,#27637,#27638,#27639,
#27640,#27641,#27642,#27643,#27644,#27645,#27646,#27647,#27648,#27649,#27650,
#27651,#27652,#27653,#27654,#27655,#27656,#27657,#27658,#27659,#27660,#27661,
#27662,#27663,#27664,#27665,#27666,#27667,#27668,#27669,#27670,#27671,#27672,
#27673,#27674,#27675,#27676,#27677,#27678,#27679,#27680,#27681,#27682,#27683,
#27684,#27685,#27686,#27687,#27688,#27689,#27690,#27691,#27692,#27693,#27694,
#27695,#27696,#27697,#27698,#27699,#27700,#27701,#27702,#27703,#27704,#27705,
#27706,#27707,#27708,#27709,#27710,#27711,#27712,#27713,#27714,#27715,#27716,
#27717,#27718,#27719,#27720,#27721,#27722,#27723,#27724,#27725,#27726,#27727,
#27728,#27729,#27730,#27731,#27732,#27733,#27734,#27735,#27736,#27737,#27738,
#27739,#27740,#27741,#27742,#27743,#27744,#27745,#27746,#27747,#27748,#27749,
#27750,#27751,#27752,#27753,#27754,#27755,#27756,#27757,#27758,#27759,#27760,
#27761,#27762,#27763,#27764,#27765,#27766,#27767,#27768,#27769,#27770,#27771,
#27772,#27773,#27774,#27775,#27776,#27777,#27778,#27779,#27780,#27781,#27782,
#27783,#27784,#27785,#27786,#27787,#27788,#27789,#27790,#27791,#27792,#27793,
#27794,#27795,#27796,#27797,#27798,#27799,#27800,#27801,#27802,#27803,#27804,
#27805,#27806,#27807,#27808,#27809,#27810,#27811,#27812,#27813,#27814,#27815,
#27816,#27817,#27818,#27819,#27820,#27821,#27822,#27823,#27824,#27825,#27826,
#27827,#27828,#27829,#27830,#27831,#27832,#27833,#27834,#27835,#27836,#27837,
#27838,#27839,#27840,#27841),.UNSPECIFIED.,.F.,.F.,(4,3,3,3,3,3,3,3,3,3,
3,3,3,3,3,3,3,3,3,3,3,3,3,3,3,3,3,3,3,3,3,3,3,3,3,3,3,3,3,3,3,3,3,3,3,3,
3,3,3,3,3,3,3,3,3,3,3,3,3,3,3,3,3,3,3,3,3,3,3,3,3,3,3,3,3,3,4),(562.345084992753,
562.437348628487,562.530118911342,562.623151742719,562.716522454311,562.74176658777,
562.825513320472,562.909156997488,562.992717741554,563.076215603511,563.159678104074,
563.243123239566,563.326569074409,563.410033669647,563.493586855069,563.577184688641,
563.660916251503,563.740750089969,563.824496822671,563.908140499687,563.991701243753,
564.07519910571,564.158661606272,564.242106741765,564.325552576607,564.409017171846,
564.492570357267,564.57616819084,564.659899753702,564.739733592168,564.82348032487,
564.907124001886,564.990684745952,565.074182607909,565.157645108472,565.241090243964,
565.324536078807,565.408000674045,565.491553859467,565.575151693039,565.658883255901,
565.738717094367,565.822463827069,565.906107504085,565.989668248151,566.073166110108,
566.156628610671,566.240073746163,566.323519581006,566.406984176244,566.490537361666,
566.574135195238,566.6578667581,566.737700596566,566.821447329268,566.905091006284,
566.988651750351,567.072149612307,567.15561211287,567.239057248362,567.322503083205,
567.405967678443,567.489520863865,567.573118697438,567.6568502603,567.736684098766,
567.819341452811,567.901896585442,567.98437060958,568.066783877203,568.149164799221,
568.231532317683,568.313905361203,568.396346362416,568.478822157388,568.561411095726,
568.628270299618),.UNSPECIFIED.);
#327=B_SPLINE_CURVE_WITH_KNOTS('',3,(#27843,#27844,#27845,#27846,#27847,
#27848,#27849,#27850,#27851,#27852,#27853,#27854,#27855,#27856,#27857,#27858,
#27859,#27860,#27861,#27862,#27863,#27864,#27865,#27866,#27867,#27868,#27869,
#27870,#27871,#27872,#27873,#27874,#27875,#27876,#27877,#27878,#27879,#27880,
#27881,#27882,#27883,#27884,#27885,#27886,#27887,#27888,#27889,#27890,#27891,
#27892,#27893,#27894,#27895,#27896,#27897,#27898,#27899,#27900,#27901,#27902,
#27903,#27904,#27905,#27906,#27907,#27908,#27909,#27910,#27911,#27912,#27913,
#27914,#27915,#27916,#27917,#27918,#27919,#27920,#27921,#27922,#27923,#27924,
#27925,#27926,#27927,#27928,#27929,#27930,#27931,#27932,#27933,#27934,#27935,
#27936,#27937,#27938,#27939,#27940,#27941,#27942,#27943,#27944,#27945,#27946,
#27947,#27948,#27949,#27950,#27951,#27952,#27953,#27954,#27955,#27956,#27957,
#27958,#27959,#27960,#27961,#27962,#27963,#27964,#27965,#27966,#27967,#27968,
#27969,#27970,#27971,#27972,#27973,#27974,#27975,#27976,#27977,#27978,#27979,
#27980,#27981,#27982,#27983,#27984,#27985,#27986,#27987,#27988,#27989,#27990,
#27991,#27992,#27993,#27994,#27995,#27996,#27997,#27998,#27999,#28000,#28001,
#28002,#28003,#28004,#28005,#28006,#28007,#28008,#28009,#28010,#28011,#28012,
#28013,#28014,#28015,#28016,#28017,#28018,#28019,#28020,#28021,#28022,#28023,
#28024,#28025,#28026,#28027,#28028,#28029,#28030,#28031,#28032,#28033,#28034,
#28035,#28036,#28037,#28038,#28039,#28040,#28041,#28042,#28043,#28044,#28045,
#28046,#28047,#28048,#28049,#28050,#28051,#28052,#28053,#28054,#28055,#28056,
#28057,#28058,#28059,#28060,#28061,#28062,#28063,#28064,#28065,#28066,#28067,
#28068,#28069,#28070,#28071),.UNSPECIFIED.,.F.,.F.,(4,3,3,3,3,3,3,3,3,3,
3,3,3,3,3,3,3,3,3,3,3,3,3,3,3,3,3,3,3,3,3,3,3,3,3,3,3,3,3,3,3,3,3,3,3,3,
3,3,3,3,3,3,3,3,3,3,3,3,3,3,3,3,3,3,3,3,3,3,3,3,3,3,3,3,3,3,4),(556.061899685394,
556.147645421542,556.23075807931,556.313867712067,556.3969926505,556.480151232029,
556.563407194035,556.646721589556,556.73015545405,556.747865574575,556.831612307277,
556.915255984293,556.998816728359,557.082314590317,557.165777090879,557.249222226372,
557.332668061214,557.416132656453,557.499685841874,557.583283675447,557.667015238309,
557.746849076774,557.830595809476,557.914239486492,557.997800230558,558.081298092515,
558.164760593078,558.24820572857,558.331651563413,558.415116158651,558.498669344073,
558.582267177646,558.665998740507,558.745832578973,558.829579311675,558.913222988691,
558.996783732757,559.080281594714,559.163744095276,559.247189230768,559.330635065611,
559.414099660849,559.497652846271,559.581250679843,559.664982242705,559.744816081172,
559.828562813874,559.91220649089,559.995767234957,560.079265096913,560.162727597476,
560.246172732968,560.329618567811,560.413083163049,560.496636348471,560.580234182043,
560.663965744905,560.743799583371,560.827546316073,560.911189993089,560.994750737156,
561.078248599113,561.161711099675,561.245156235168,561.32860207001,561.412066665249,
561.49561985067,561.579217684243,561.662949247105,561.742783085571,561.827693316259,
561.912491884059,561.997195483401,562.084167860694,562.168721138886,562.256903065729,
562.345084992573),.UNSPECIFIED.);
#328=B_SPLINE_CURVE_WITH_KNOTS('',3,(#28073,#28074,#28075,#28076,#28077,
#28078,#28079,#28080,#28081,#28082),.UNSPECIFIED.,.F.,.F.,(4,1,1,1,1,1,
1,4),(549.778717730147,550.75396456138,551.752948063579,552.751931565778,
553.750915067977,554.749898570176,555.748882072376,556.061893235856),
 .UNSPECIFIED.);
#329=B_SPLINE_CURVE_WITH_KNOTS('',3,(#28084,#28085,#28086,#28087,#28088,
#28089,#28090,#28091,#28092,#28093,#28094,#28095,#28096,#28097,#28098,#28099,
#28100,#28101,#28102,#28103,#28104,#28105,#28106,#28107,#28108,#28109,#28110,
#28111,#28112,#28113,#28114,#28115,#28116,#28117,#28118,#28119,#28120,#28121,
#28122,#28123,#28124,#28125,#28126,#28127,#28128,#28129,#28130,#28131,#28132,
#28133,#28134,#28135,#28136,#28137,#28138,#28139,#28140,#28141,#28142,#28143,
#28144,#28145,#28146,#28147,#28148,#28149,#28150,#28151,#28152,#28153,#28154,
#28155,#28156,#28157,#28158,#28159,#28160,#28161,#28162,#28163,#28164,#28165,
#28166,#28167,#28168,#28169,#28170,#28171,#28172,#28173,#28174,#28175,#28176,
#28177,#28178,#28179,#28180,#28181,#28182,#28183,#28184,#28185,#28186,#28187,
#28188,#28189,#28190,#28191,#28192,#28193,#28194,#28195,#28196,#28197,#28198,
#28199,#28200,#28201,#28202,#28203,#28204,#28205,#28206,#28207,#28208,#28209,
#28210,#28211,#28212,#28213,#28214,#28215,#28216,#28217,#28218,#28219,#28220,
#28221,#28222,#28223,#28224,#28225,#28226,#28227,#28228,#28229,#28230,#28231,
#28232,#28233,#28234,#28235,#28236,#28237,#28238,#28239,#28240,#28241,#28242,
#28243,#28244,#28245,#28246,#28247,#28248,#28249,#28250,#28251,#28252,#28253,
#28254,#28255,#28256,#28257,#28258,#28259,#28260,#28261,#28262,#28263,#28264,
#28265,#28266,#28267,#28268,#28269,#28270,#28271,#28272,#28273,#28274,#28275,
#28276,#28277,#28278,#28279,#28280,#28281,#28282,#28283,#28284,#28285,#28286,
#28287,#28288,#28289,#28290,#28291,#28292,#28293,#28294,#28295,#28296,#28297,
#28298,#28299,#28300,#28301,#28302,#28303,#28304,#28305,#28306,#28307,#28308,
#28309,#28310,#28311,#28312),.UNSPECIFIED.,.F.,.F.,(4,3,3,3,3,3,3,3,3,3,
3,3,3,3,3,3,3,3,3,3,3,3,3,3,3,3,3,3,3,3,3,3,3,3,3,3,3,3,3,3,3,3,3,3,3,3,
3,3,3,3,3,3,3,3,3,3,3,3,3,3,3,3,3,3,3,3,3,3,3,3,3,3,3,3,3,3,4),(543.495529071195,
543.600349959761,543.70712252169,543.761080045986,543.844826778688,543.928470455704,
544.012031199771,544.095529061728,544.178991562291,544.262436697784,544.345882532627,
544.429347127865,544.512900313287,544.59649814686,544.680229709723,544.760063548185,
544.843810280887,544.927453957903,545.011014701969,545.094512563926,545.177975064488,
545.261420199981,545.344866034824,545.428330630062,545.511883815483,545.595481649056,
545.679213211918,545.759047050384,545.842793783086,545.926437460102,546.009998204168,
546.093496066124,546.176958566687,546.260403702179,546.343849537022,546.427314132259,
546.510867317681,546.594465151254,546.678196714115,546.758030552583,546.841777285285,
546.925420962301,547.008981706367,547.092479568324,547.175942068887,547.259387204379,
547.342833039222,547.42629763446,547.509850819882,547.593448653455,547.677180216316,
547.757014054782,547.840760787484,547.9244044645,548.007965208567,548.091463070524,
548.174925571086,548.258370706579,548.341816541422,548.42528113666,548.508834322082,
548.592432155655,548.676163718517,548.755997556982,548.839744289684,548.9233879667,
549.006948710767,549.090446572724,549.173909073286,549.257354208779,549.340800043622,
549.42426463886,549.507817824282,549.591415657855,549.675147220717,549.754981059181,
549.778714378214),.UNSPECIFIED.);
#330=B_SPLINE_CURVE_WITH_KNOTS('',3,(#28314,#28315,#28316,#28317,#28318,
#28319,#28320,#28321,#28322,#28323,#28324,#28325,#28326,#28327,#28328,#28329,
#28330,#28331,#28332,#28333,#28334,#28335,#28336,#28337,#28338,#28339,#28340,
#28341,#28342,#28343,#28344,#28345,#28346,#28347,#28348,#28349,#28350,#28351,
#28352,#28353,#28354,#28355,#28356,#28357,#28358,#28359,#28360,#28361,#28362,
#28363,#28364,#28365,#28366,#28367,#28368,#28369,#28370,#28371,#28372,#28373,
#28374,#28375,#28376,#28377,#28378,#28379,#28380,#28381,#28382,#28383,#28384,
#28385,#28386,#28387,#28388,#28389,#28390,#28391,#28392,#28393,#28394,#28395,
#28396,#28397,#28398,#28399,#28400,#28401,#28402,#28403,#28404,#28405,#28406,
#28407,#28408,#28409,#28410,#28411,#28412,#28413,#28414,#28415,#28416,#28417,
#28418,#28419,#28420,#28421,#28422,#28423,#28424,#28425,#28426,#28427,#28428,
#28429,#28430,#28431,#28432,#28433,#28434,#28435,#28436,#28437,#28438,#28439,
#28440,#28441,#28442,#28443,#28444,#28445,#28446,#28447,#28448,#28449,#28450,
#28451,#28452,#28453,#28454,#28455,#28456,#28457,#28458,#28459,#28460,#28461,
#28462,#28463,#28464,#28465,#28466,#28467,#28468,#28469,#28470,#28471,#28472,
#28473,#28474,#28475,#28476,#28477,#28478,#28479,#28480,#28481,#28482,#28483,
#28484,#28485,#28486,#28487,#28488,#28489,#28490,#28491,#28492,#28493,#28494,
#28495,#28496,#28497,#28498,#28499,#28500,#28501,#28502,#28503,#28504,#28505,
#28506,#28507,#28508,#28509,#28510,#28511,#28512,#28513,#28514,#28515,#28516,
#28517,#28518,#28519,#28520,#28521,#28522,#28523,#28524,#28525,#28526,#28527,
#28528,#28529,#28530,#28531,#28532,#28533,#28534,#28535,#28536,#28537,#28538,
#28539,#28540,#28541,#28542),.UNSPECIFIED.,.F.,.F.,(4,3,3,3,3,3,3,3,3,3,
3,3,3,3,3,3,3,3,3,3,3,3,3,3,3,3,3,3,3,3,3,3,3,3,3,3,3,3,3,3,3,3,3,3,3,3,
3,3,3,3,3,3,3,3,3,3,3,3,3,3,3,3,3,3,3,3,3,3,3,3,3,3,3,3,3,3,4),(537.212343763855,
537.298000378494,537.383712338006,537.469493659904,537.55542022831,537.641428057268,
537.727592604259,537.767179032791,537.850925765493,537.934569442509,538.018130186575,
538.101628048532,538.185090549094,538.268535684586,538.351981519429,538.435446114667,
538.518999300089,538.602597133661,538.686328696523,538.76616253499,538.849909267692,
538.933552944708,539.017113688774,539.100611550731,539.184074051294,539.267519186786,
539.350965021629,539.434429616867,539.517982802289,539.601580635861,539.685312198723,
539.765146037189,539.848892769891,539.932536446907,540.016097190973,540.09959505293,
540.183057553493,540.266502688985,540.349948523828,540.433413119066,540.516966304488,
540.60056413806,540.684295700922,540.764129539388,540.84787627209,540.931519949106,
541.015080693172,541.098578555128,541.182041055691,541.265486191183,541.348932026026,
541.432396621264,541.515949806686,541.599547640258,541.68327920312,541.763113041587,
541.846859774289,541.930503451305,542.014064195372,542.09756205733,542.181024557892,
542.264469693385,542.347915528228,542.431380123467,542.514933308888,542.598531142461,
542.682262705323,542.762096543787,542.845014125629,542.927800991536,543.010512696025,
543.093168093423,543.175785990596,543.258405489438,543.341022571314,543.423694512478,
543.495529071035),.UNSPECIFIED.);
#331=B_SPLINE_CURVE_WITH_KNOTS('',3,(#28544,#28545,#28546,#28547,#28548,
#28549,#28550,#28551,#28552,#28553,#28554,#28555,#28556,#28557,#28558,#28559,
#28560,#28561,#28562,#28563,#28564,#28565,#28566,#28567,#28568,#28569,#28570,
#28571,#28572,#28573,#28574,#28575,#28576,#28577,#28578,#28579,#28580,#28581,
#28582,#28583,#28584,#28585,#28586,#28587,#28588,#28589,#28590,#28591,#28592,
#28593,#28594,#28595,#28596,#28597,#28598,#28599,#28600,#28601,#28602,#28603,
#28604,#28605,#28606,#28607,#28608,#28609,#28610,#28611,#28612,#28613,#28614,
#28615,#28616,#28617,#28618,#28619,#28620,#28621,#28622,#28623,#28624,#28625,
#28626,#28627,#28628,#28629,#28630,#28631,#28632,#28633,#28634,#28635,#28636,
#28637,#28638,#28639,#28640,#28641,#28642,#28643,#28644,#28645,#28646,#28647,
#28648,#28649,#28650,#28651,#28652,#28653,#28654,#28655,#28656,#28657,#28658,
#28659,#28660,#28661,#28662,#28663,#28664,#28665,#28666,#28667,#28668,#28669,
#28670,#28671,#28672,#28673,#28674,#28675,#28676,#28677,#28678,#28679,#28680,
#28681,#28682,#28683,#28684,#28685,#28686,#28687,#28688,#28689,#28690,#28691,
#28692,#28693,#28694,#28695,#28696,#28697,#28698,#28699,#28700,#28701,#28702,
#28703,#28704,#28705,#28706,#28707,#28708,#28709,#28710,#28711,#28712,#28713,
#28714,#28715,#28716,#28717,#28718,#28719,#28720,#28721,#28722,#28723,#28724,
#28725,#28726,#28727,#28728,#28729,#28730,#28731,#28732,#28733,#28734,#28735,
#28736,#28737,#28738,#28739,#28740,#28741,#28742,#28743,#28744,#28745,#28746,
#28747,#28748,#28749,#28750,#28751,#28752,#28753,#28754,#28755,#28756,#28757,
#28758,#28759,#28760,#28761,#28762,#28763,#28764,#28765,#28766,#28767,#28768,
#28769,#28770,#28771,#28772),.UNSPECIFIED.,.F.,.F.,(4,3,3,3,3,3,3,3,3,3,
3,3,3,3,3,3,3,3,3,3,3,3,3,3,3,3,3,3,3,3,3,3,3,3,3,3,3,3,3,3,3,3,3,3,3,3,
3,3,3,3,3,3,3,3,3,3,3,3,3,3,3,3,3,3,3,3,3,3,3,3,3,3,3,3,3,3,4),(530.929158456783,
531.01156105809,531.093882835983,531.178807233935,531.261038216809,531.343257242855,
531.42548333556,531.507735522145,531.590076053576,531.6724696604,531.754977052498,
531.773278019596,531.857024752298,531.940668429314,532.02422917338,532.107727035337,
532.191189535899,532.274634671391,532.358080506234,532.441545101472,532.525098286894,
532.608696120467,532.692427683329,532.772261521795,532.856008254497,532.939651931513,
533.02321267558,533.106710537537,533.190173038099,533.273618173592,533.357064008434,
533.440528603673,533.524081789094,533.607679622667,533.691411185529,533.771245023994,
533.854991756696,533.938635433712,534.022196177778,534.105694039735,534.189156540297,
534.272601675789,534.356047510632,534.43951210587,534.523065291292,534.606663124864,
534.690394687726,534.770228526193,534.853975258895,534.937618935911,535.021179679977,
535.104677541934,535.188140042496,535.271585177988,535.355031012831,535.438495608069,
535.522048793491,535.605646627064,535.689378189925,535.769212028392,535.852958761094,
535.93660243811,536.020163182177,536.103661044133,536.187123544696,536.270568680188,
536.354014515031,536.437479110269,536.521032295691,536.604630129264,536.688361692126,
536.768195530591,536.85877152174,536.949048084385,537.039143045008,537.128947971728,
537.212343763737),.UNSPECIFIED.);
#332=B_SPLINE_CURVE_WITH_KNOTS('',3,(#28774,#28775,#28776,#28777,#28778,
#28779,#28780,#28781,#28782,#28783,#28784,#28785,#28786,#28787,#28788,#28789,
#28790,#28791,#28792,#28793,#28794,#28795,#28796,#28797,#28798,#28799,#28800,
#28801,#28802,#28803,#28804,#28805,#28806,#28807,#28808,#28809,#28810,#28811,
#28812,#28813,#28814,#28815,#28816,#28817,#28818,#28819,#28820,#28821,#28822,
#28823,#28824,#28825,#28826,#28827,#28828,#28829,#28830,#28831,#28832,#28833,
#28834,#28835,#28836,#28837,#28838,#28839,#28840,#28841,#28842,#28843,#28844,
#28845,#28846,#28847,#28848,#28849,#28850,#28851,#28852,#28853,#28854,#28855,
#28856,#28857,#28858,#28859,#28860,#28861,#28862,#28863,#28864,#28865,#28866,
#28867,#28868,#28869,#28870,#28871,#28872,#28873,#28874,#28875,#28876,#28877,
#28878,#28879,#28880,#28881,#28882,#28883,#28884,#28885,#28886,#28887,#28888,
#28889,#28890,#28891,#28892,#28893,#28894,#28895,#28896,#28897,#28898,#28899,
#28900,#28901,#28902,#28903,#28904,#28905,#28906,#28907,#28908,#28909,#28910,
#28911,#28912,#28913,#28914,#28915,#28916,#28917,#28918,#28919,#28920,#28921,
#28922,#28923,#28924,#28925,#28926,#28927,#28928,#28929,#28930,#28931,#28932,
#28933,#28934,#28935,#28936,#28937,#28938,#28939,#28940,#28941,#28942,#28943,
#28944,#28945,#28946,#28947,#28948,#28949,#28950,#28951,#28952,#28953,#28954,
#28955,#28956,#28957,#28958,#28959,#28960,#28961,#28962,#28963,#28964,#28965,
#28966,#28967,#28968,#28969,#28970,#28971,#28972,#28973,#28974,#28975,#28976,
#28977,#28978,#28979,#28980,#28981,#28982,#28983,#28984,#28985,#28986,#28987,
#28988,#28989,#28990,#28991,#28992,#28993,#28994,#28995,#28996,#28997,#28998,
#28999),.UNSPECIFIED.,.F.,.F.,(4,3,3,3,3,3,3,3,3,3,3,3,3,3,3,3,3,3,3,3,
3,3,3,3,3,3,3,3,3,3,3,3,3,3,3,3,3,3,3,3,3,3,3,3,3,3,3,3,3,3,3,3,3,3,3,3,
3,3,3,3,3,3,3,3,3,3,3,3,3,3,3,3,3,3,3,4),(524.645973149496,524.780393504201,
524.864140236903,524.947783913919,525.031344657985,525.114842519942,525.198305020505,
525.281750155997,525.36519599084,525.448660586078,525.5322137715,525.615811605073,
525.699543167934,525.779377006401,525.863123739103,525.946767416119,526.030328160185,
526.113826022142,526.197288522705,526.280733658197,526.36417949304,526.447644088278,
526.5311972737,526.614795107272,526.698526670134,526.7783605086,526.862107241302,
526.945750918318,527.029311662384,527.112809524341,527.196272024904,527.279717160396,
527.363162995239,527.446627590477,527.530180775899,527.613778609471,527.697510172333,
527.777344010799,527.861090743501,527.944734420517,528.028295164583,528.11179302654,
528.195255527103,528.278700662595,528.362146497438,528.445611092676,528.529164278098,
528.61276211167,528.696493674532,528.776327512998,528.8600742457,528.943717922716,
529.027278666782,529.110776528739,529.194239029301,529.277684164794,529.361129999636,
529.444594594874,529.528147780296,529.611745613869,529.69547717673,529.775311015197,
529.859057747899,529.942701424915,530.026262168981,530.109760030938,530.193222531501,
530.276667666993,530.360113501836,530.443578097074,530.527131282496,530.610729116068,
530.69446067893,530.774294517396,530.913405606285,530.929158456676),
 .UNSPECIFIED.);
#333=B_SPLINE_CURVE_WITH_KNOTS('',3,(#29001,#29002,#29003,#29004,#29005,
#29006,#29007,#29008,#29009,#29010,#29011,#29012,#29013,#29014,#29015,#29016,
#29017,#29018,#29019,#29020,#29021,#29022,#29023,#29024,#29025,#29026,#29027,
#29028,#29029,#29030,#29031,#29032,#29033,#29034,#29035,#29036,#29037,#29038,
#29039,#29040,#29041,#29042,#29043,#29044,#29045,#29046,#29047,#29048,#29049,
#29050,#29051,#29052,#29053,#29054,#29055,#29056,#29057,#29058,#29059,#29060,
#29061,#29062,#29063,#29064,#29065,#29066,#29067,#29068,#29069,#29070,#29071,
#29072,#29073,#29074,#29075,#29076,#29077,#29078,#29079,#29080,#29081,#29082,
#29083,#29084,#29085,#29086,#29087,#29088,#29089,#29090,#29091,#29092,#29093,
#29094,#29095,#29096,#29097,#29098,#29099,#29100,#29101,#29102,#29103,#29104,
#29105,#29106,#29107,#29108,#29109,#29110,#29111,#29112,#29113,#29114,#29115,
#29116,#29117,#29118,#29119,#29120,#29121,#29122,#29123,#29124,#29125,#29126,
#29127,#29128,#29129,#29130,#29131,#29132,#29133,#29134,#29135,#29136,#29137,
#29138,#29139,#29140,#29141,#29142,#29143,#29144,#29145,#29146,#29147,#29148,
#29149,#29150,#29151,#29152,#29153,#29154,#29155,#29156,#29157,#29158,#29159,
#29160,#29161,#29162,#29163,#29164,#29165,#29166,#29167,#29168,#29169,#29170,
#29171,#29172,#29173,#29174,#29175,#29176,#29177,#29178,#29179,#29180,#29181,
#29182,#29183,#29184,#29185,#29186,#29187,#29188,#29189,#29190,#29191,#29192,
#29193,#29194,#29195,#29196,#29197,#29198,#29199,#29200,#29201,#29202,#29203,
#29204,#29205,#29206,#29207,#29208,#29209,#29210,#29211,#29212,#29213,#29214,
#29215,#29216,#29217,#29218,#29219,#29220,#29221,#29222,#29223,#29224,#29225,
#29226,#29227,#29228,#29229),.UNSPECIFIED.,.F.,.F.,(4,3,3,3,3,3,3,3,3,3,
3,3,3,3,3,3,3,3,3,3,3,3,3,3,3,3,3,3,3,3,3,3,3,3,3,3,3,3,3,3,3,3,3,3,3,3,
3,3,3,3,3,3,3,3,3,3,3,3,3,3,3,3,3,3,3,3,3,3,3,3,3,3,3,3,3,3,4),(518.362787842463,
518.453523730853,518.544661312336,518.636003322358,518.727651533168,518.786492491007,
518.870239223709,518.953882900725,519.037443644791,519.120941506748,519.204404007311,
519.287849142803,519.371294977646,519.454759572884,519.538312758306,519.621910591878,
519.70564215474,519.785475993206,519.869222725908,519.952866402924,520.03642714699,
520.119925008947,520.203387509509,520.286832645001,520.370278479844,520.453743075082,
520.537296260504,520.620894094076,520.704625656938,520.784459495405,520.868206228107,
520.951849905123,521.03541064919,521.118908511146,521.202371011709,521.285816147201,
521.369261982044,521.452726577282,521.536279762704,521.619877596277,521.703609159139,
521.783442997604,521.867189730306,521.950833407322,522.034394151388,522.117892013345,
522.201354513907,522.284799649399,522.368245484242,522.45171007948,522.535263264902,
522.618861098475,522.702592661336,522.782426499803,522.866173232505,522.949816909521,
523.033377653587,523.116875515544,523.200338016107,523.283783151599,523.367228986442,
523.45069358168,523.534246767102,523.617844600674,523.701576163536,523.781410002002,
523.863956676188,523.946401108076,524.02876449323,524.11106650296,524.193336204663,
524.275592609193,524.357854713714,524.440179777105,524.522540120567,524.605000346848,
524.645973149371),.UNSPECIFIED.);
#334=B_SPLINE_CURVE_WITH_KNOTS('',3,(#29231,#29232,#29233,#29234,#29235,
#29236,#29237,#29238,#29239,#29240,#29241,#29242,#29243,#29244,#29245,#29246,
#29247,#29248,#29249,#29250,#29251,#29252,#29253,#29254,#29255,#29256,#29257,
#29258,#29259,#29260,#29261,#29262,#29263,#29264,#29265,#29266,#29267,#29268,
#29269,#29270,#29271,#29272,#29273,#29274,#29275,#29276,#29277,#29278,#29279,
#29280,#29281,#29282,#29283,#29284,#29285,#29286,#29287,#29288,#29289,#29290,
#29291,#29292,#29293,#29294,#29295,#29296,#29297,#29298,#29299,#29300,#29301,
#29302,#29303,#29304,#29305,#29306,#29307,#29308,#29309,#29310,#29311,#29312,
#29313,#29314,#29315,#29316,#29317,#29318,#29319,#29320,#29321,#29322,#29323,
#29324,#29325,#29326,#29327,#29328,#29329,#29330,#29331,#29332,#29333,#29334,
#29335,#29336,#29337,#29338,#29339,#29340,#29341,#29342,#29343,#29344,#29345,
#29346,#29347,#29348,#29349,#29350,#29351,#29352,#29353,#29354,#29355,#29356,
#29357,#29358,#29359,#29360,#29361,#29362,#29363,#29364,#29365,#29366,#29367,
#29368,#29369,#29370,#29371,#29372,#29373,#29374,#29375,#29376,#29377,#29378,
#29379,#29380,#29381,#29382,#29383,#29384,#29385,#29386,#29387,#29388,#29389,
#29390,#29391,#29392,#29393,#29394,#29395,#29396,#29397,#29398,#29399,#29400,
#29401,#29402,#29403,#29404,#29405,#29406,#29407,#29408,#29409,#29410,#29411,
#29412,#29413,#29414,#29415,#29416,#29417,#29418,#29419,#29420,#29421,#29422,
#29423,#29424,#29425,#29426,#29427,#29428,#29429,#29430,#29431,#29432,#29433,
#29434,#29435,#29436,#29437,#29438,#29439,#29440,#29441,#29442,#29443,#29444,
#29445,#29446,#29447,#29448,#29449,#29450,#29451,#29452,#29453,#29454,#29455,
#29456,#29457,#29458,#29459),.UNSPECIFIED.,.F.,.F.,(4,3,3,3,3,3,3,3,3,3,
3,3,3,3,3,3,3,3,3,3,3,3,3,3,3,3,3,3,3,3,3,3,3,3,3,3,3,3,3,3,3,3,3,3,3,3,
3,3,3,3,3,3,3,3,3,3,3,3,3,3,3,3,3,3,3,3,3,3,3,3,3,3,3,3,3,3,4),(512.079602535137,
512.162447478009,512.245261499868,512.328061801061,512.410866989149,512.493695671928,
512.576614950116,512.659584111197,512.742679148104,512.792591477812,512.876338210514,
512.95998188753,513.043542631596,513.127040493553,513.210502994115,513.293948129608,
513.37739396445,513.460858559689,513.544411745111,513.628009578683,513.711741141545,
513.791574980011,513.875321712713,513.958965389729,514.042526133795,514.126023995752,
514.209486496315,514.292931631807,514.37637746665,514.459842061888,514.54339524731,
514.626993080883,514.710724643744,514.79055848221,514.874305214912,514.957948891928,
515.041509635994,515.125007497951,515.208469998513,515.291915134005,515.375360968848,
515.458825564086,515.542378749508,515.625976583081,515.709708145942,515.789541984409,
515.873288717111,515.956932394127,516.040493138193,516.12399100015,516.207453500713,
516.290898636205,516.374344471048,516.457809066286,516.541362251708,516.62496008528,
516.708691648142,516.788525486608,516.87227221931,516.955915896326,517.039476640392,
517.122974502349,517.206437002912,517.289882138404,517.373327973246,517.456792568485,
517.540345753906,517.623943587479,517.707675150341,517.787508988807,517.873089538018,
517.958551346935,518.043909947176,518.129158670079,518.21434289738,518.299470899801,
518.362787842316),.UNSPECIFIED.);
#335=B_SPLINE_CURVE_WITH_KNOTS('',3,(#29461,#29462,#29463,#29464,#29465,
#29466,#29467,#29468,#29469,#29470,#29471,#29472,#29473,#29474,#29475,#29476,
#29477,#29478,#29479,#29480,#29481,#29482,#29483,#29484,#29485,#29486,#29487,
#29488,#29489,#29490,#29491,#29492,#29493,#29494,#29495,#29496,#29497,#29498,
#29499,#29500,#29501,#29502,#29503,#29504,#29505,#29506,#29507,#29508,#29509,
#29510,#29511,#29512,#29513,#29514,#29515,#29516,#29517,#29518,#29519,#29520,
#29521,#29522,#29523,#29524,#29525,#29526,#29527,#29528,#29529,#29530,#29531,
#29532,#29533,#29534,#29535,#29536,#29537,#29538,#29539,#29540,#29541,#29542,
#29543,#29544,#29545,#29546,#29547,#29548,#29549,#29550,#29551,#29552,#29553,
#29554,#29555,#29556,#29557,#29558,#29559,#29560,#29561,#29562,#29563,#29564,
#29565,#29566,#29567,#29568,#29569,#29570,#29571,#29572,#29573,#29574,#29575,
#29576,#29577,#29578,#29579,#29580,#29581,#29582,#29583,#29584,#29585,#29586,
#29587,#29588,#29589,#29590,#29591,#29592,#29593,#29594,#29595,#29596,#29597,
#29598,#29599,#29600,#29601,#29602,#29603,#29604,#29605,#29606,#29607,#29608,
#29609,#29610,#29611,#29612,#29613,#29614,#29615,#29616,#29617,#29618,#29619,
#29620,#29621,#29622,#29623,#29624,#29625,#29626,#29627,#29628,#29629,#29630,
#29631,#29632,#29633,#29634,#29635,#29636,#29637,#29638,#29639,#29640,#29641,
#29642,#29643,#29644,#29645,#29646,#29647,#29648,#29649,#29650,#29651,#29652,
#29653,#29654,#29655,#29656,#29657,#29658,#29659,#29660,#29661,#29662,#29663,
#29664,#29665,#29666,#29667,#29668,#29669,#29670,#29671,#29672,#29673,#29674,
#29675,#29676,#29677,#29678,#29679,#29680,#29681,#29682,#29683,#29684,#29685,
#29686,#29687,#29688,#29689),.UNSPECIFIED.,.F.,.F.,(4,3,3,3,3,3,3,3,3,3,
3,3,3,3,3,3,3,3,3,3,3,3,3,3,3,3,3,3,3,3,3,3,3,3,3,3,3,3,3,3,3,3,3,3,3,3,
3,3,3,3,3,3,3,3,3,3,3,3,3,3,3,3,3,3,3,3,3,3,3,3,3,3,3,3,3,3,4),(505.796417227957,
505.799706962417,505.883453695119,505.967097372135,506.050658116202,506.134155978159,
506.217618478722,506.301063614214,506.384509449057,506.467974044295,506.551527229718,
506.63512506329,506.718856626153,506.798690464617,506.882437197319,506.966080874335,
507.049641618401,507.133139480358,507.21660198092,507.300047116413,507.383492951256,
507.466957546494,507.550510731915,507.634108565488,507.71784012835,507.797673966816,
507.881420699518,507.965064376533,508.0486251206,508.132122982556,508.215585483119,
508.299030618611,508.382476453454,508.465941048692,508.549494234113,508.633092067686,
508.716823630547,508.796657469015,508.880404201717,508.964047878733,509.0476086228,
509.131106484756,509.214568985319,509.298014120812,509.381459955655,509.464924550893,
509.548477736315,509.632075569888,509.71580713275,509.795640971214,509.879387703916,
509.963031380931,510.046592124998,510.130089986954,510.213552487517,510.296997623009,
510.380443457852,510.46390805309,510.547461238512,510.631059072084,510.714790634946,
510.794624473413,510.878371206115,510.962014883131,511.045575627198,511.129073489155,
511.212535989718,511.295981125211,511.379426960054,511.462891555292,511.546444740714,
511.630042574287,511.713774137149,511.793607975613,511.897484169068,511.99988621917,
512.079602535015),.UNSPECIFIED.);
#336=B_SPLINE_CURVE_WITH_KNOTS('',3,(#29691,#29692,#29693,#29694,#29695,
#29696,#29697,#29698,#29699,#29700,#29701,#29702,#29703,#29704,#29705,#29706,
#29707,#29708,#29709,#29710,#29711,#29712,#29713,#29714,#29715,#29716,#29717,
#29718,#29719,#29720,#29721,#29722,#29723,#29724,#29725,#29726,#29727,#29728,
#29729,#29730,#29731,#29732,#29733,#29734,#29735,#29736,#29737,#29738,#29739,
#29740,#29741,#29742,#29743,#29744,#29745,#29746,#29747,#29748,#29749,#29750,
#29751,#29752,#29753,#29754,#29755,#29756,#29757,#29758,#29759,#29760,#29761,
#29762,#29763,#29764,#29765,#29766,#29767,#29768,#29769,#29770,#29771,#29772,
#29773,#29774,#29775,#29776,#29777,#29778,#29779,#29780,#29781,#29782,#29783,
#29784,#29785,#29786,#29787,#29788,#29789,#29790,#29791,#29792,#29793,#29794,
#29795,#29796,#29797,#29798,#29799,#29800,#29801,#29802,#29803,#29804,#29805,
#29806,#29807,#29808,#29809,#29810,#29811,#29812,#29813,#29814,#29815,#29816,
#29817,#29818,#29819,#29820,#29821,#29822,#29823,#29824,#29825,#29826,#29827,
#29828,#29829,#29830,#29831,#29832,#29833,#29834,#29835,#29836,#29837,#29838,
#29839,#29840,#29841,#29842,#29843,#29844,#29845,#29846,#29847,#29848,#29849,
#29850,#29851,#29852,#29853,#29854,#29855,#29856,#29857,#29858,#29859,#29860,
#29861,#29862,#29863,#29864,#29865,#29866,#29867,#29868,#29869,#29870,#29871,
#29872,#29873,#29874,#29875,#29876,#29877,#29878,#29879,#29880,#29881,#29882,
#29883,#29884,#29885,#29886,#29887,#29888,#29889,#29890,#29891,#29892,#29893,
#29894,#29895,#29896,#29897,#29898,#29899,#29900,#29901,#29902,#29903,#29904,
#29905,#29906,#29907,#29908,#29909,#29910,#29911,#29912,#29913,#29914,#29915,
#29916),.UNSPECIFIED.,.F.,.F.,(4,3,3,3,3,3,3,3,3,3,3,3,3,3,3,3,3,3,3,3,
3,3,3,3,3,3,3,3,3,3,3,3,3,3,3,3,3,3,3,3,3,3,3,3,3,3,3,3,3,3,3,3,3,3,3,3,
3,3,3,3,3,3,3,3,3,3,3,3,3,3,3,3,3,3,3,4),(499.513231920912,499.614580001576,
499.717352199052,499.805805949222,499.889552681924,499.97319635894,500.056757103006,
500.140254964963,500.223717465526,500.307162601018,500.390608435861,500.474073031099,
500.557626216521,500.641224050093,500.724955612955,500.804789451422,500.888536184124,
500.97217986114,501.055740605206,501.139238467163,501.222700967726,501.306146103218,
501.389591938061,501.473056533299,501.556609718721,501.640207552293,501.723939115155,
501.803772953621,501.887519686323,501.971163363339,502.054724107405,502.138221969362,
502.221684469925,502.305129605417,502.38857544026,502.472040035498,502.55559322092,
502.639191054493,502.722922617355,502.80275645582,502.886503188522,502.970146865538,
503.053707609604,503.137205471561,503.220667972123,503.304113107615,503.387558942458,
503.471023537696,503.554576723118,503.63817455669,503.721906119552,503.801739958019,
503.885486690721,503.969130367737,504.052691111803,504.13618897376,504.219651474323,
504.303096609815,504.386542444658,504.470007039896,504.553560225318,504.63715805889,
504.720889621752,504.800723460218,504.884420596488,504.968014701809,505.051525952777,
505.134974453708,505.218387813693,505.301784027289,505.385181206877,505.468597461663,
505.552102310251,505.635652182034,505.719334882353,505.796417227828),
 .UNSPECIFIED.);
#337=B_SPLINE_CURVE_WITH_KNOTS('',3,(#29918,#29919,#29920,#29921,#29922,
#29923,#29924,#29925,#29926,#29927,#29928,#29929,#29930,#29931,#29932,#29933,
#29934,#29935,#29936,#29937,#29938,#29939,#29940,#29941,#29942,#29943,#29944,
#29945,#29946,#29947,#29948,#29949,#29950,#29951,#29952,#29953,#29954,#29955,
#29956,#29957,#29958,#29959,#29960,#29961,#29962,#29963,#29964,#29965,#29966,
#29967,#29968,#29969,#29970,#29971,#29972,#29973,#29974,#29975,#29976,#29977,
#29978,#29979,#29980,#29981,#29982,#29983,#29984,#29985,#29986,#29987,#29988,
#29989,#29990,#29991,#29992,#29993,#29994,#29995,#29996,#29997,#29998,#29999,
#30000,#30001,#30002,#30003,#30004,#30005,#30006,#30007,#30008,#30009,#30010,
#30011,#30012,#30013,#30014,#30015,#30016,#30017,#30018,#30019,#30020,#30021,
#30022,#30023,#30024,#30025,#30026,#30027,#30028,#30029,#30030,#30031,#30032,
#30033,#30034,#30035,#30036,#30037,#30038,#30039,#30040,#30041,#30042,#30043,
#30044,#30045,#30046,#30047,#30048,#30049,#30050,#30051,#30052,#30053,#30054,
#30055,#30056,#30057,#30058,#30059,#30060,#30061,#30062,#30063,#30064,#30065,
#30066,#30067,#30068,#30069,#30070,#30071,#30072,#30073,#30074,#30075,#30076,
#30077,#30078,#30079,#30080,#30081,#30082,#30083,#30084,#30085,#30086,#30087,
#30088,#30089,#30090,#30091,#30092,#30093,#30094,#30095,#30096,#30097,#30098,
#30099,#30100,#30101,#30102,#30103,#30104,#30105,#30106,#30107,#30108,#30109,
#30110,#30111,#30112,#30113,#30114,#30115,#30116,#30117,#30118,#30119,#30120,
#30121,#30122,#30123,#30124,#30125,#30126,#30127,#30128,#30129,#30130,#30131,
#30132,#30133,#30134,#30135,#30136,#30137,#30138,#30139,#30140,#30141,#30142,
#30143,#30144,#30145,#30146),.UNSPECIFIED.,.F.,.F.,(4,3,3,3,3,3,3,3,3,3,
3,3,3,3,3,3,3,3,3,3,3,3,3,3,3,3,3,3,3,3,3,3,3,3,3,3,3,3,3,3,3,3,3,3,3,3,
3,3,3,3,3,3,3,3,3,3,3,3,3,3,3,3,3,3,3,3,3,3,3,3,3,3,3,3,3,3,4),(493.230046613598,
493.315013376264,493.400014227616,493.485064766745,493.570242771312,493.655487738022,
493.740890152444,493.811904936027,493.895651668729,493.979295345745,494.062856089812,
494.146353951769,494.229816452331,494.313261587824,494.396707422666,494.480172017904,
494.563725203326,494.647323036899,494.731054599761,494.810888438227,494.894635170929,
494.978278847945,495.061839592012,495.145337453968,495.228799954531,495.312245090023,
495.395690924866,495.479155520104,495.562708705526,495.646306539099,495.73003810196,
495.809871940426,495.893618673128,495.977262350144,496.06082309421,496.144320956166,
496.227783456729,496.311228592221,496.394674427064,496.478139022302,496.561692207724,
496.645290041296,496.729021604158,496.808855442625,496.892602175327,496.976245852343,
497.059806596409,497.143304458366,497.226766958929,497.310212094421,497.393657929264,
497.477122524502,497.560675709924,497.644273543496,497.728005106358,497.807838944824,
497.891585677526,497.975229354542,498.058790098609,498.142287960565,498.225750461128,
498.30919559662,498.392641431463,498.476106026701,498.559659212123,498.643257045696,
498.726988608558,498.806822447023,498.890011507484,498.973066630021,499.056044292387,
499.138963145046,499.221841791247,499.304713405022,499.387580210261,499.470486066474,
499.513231920778),.UNSPECIFIED.);
#338=B_SPLINE_CURVE_WITH_KNOTS('',3,(#30148,#30149,#30150,#30151,#30152,
#30153,#30154,#30155,#30156,#30157,#30158,#30159,#30160,#30161,#30162,#30163,
#30164,#30165,#30166,#30167,#30168,#30169,#30170,#30171,#30172,#30173,#30174,
#30175,#30176,#30177,#30178,#30179,#30180,#30181,#30182,#30183,#30184,#30185,
#30186,#30187,#30188,#30189,#30190,#30191,#30192,#30193,#30194,#30195,#30196,
#30197,#30198,#30199,#30200,#30201,#30202,#30203,#30204,#30205,#30206,#30207,
#30208,#30209,#30210,#30211,#30212,#30213,#30214,#30215,#30216,#30217,#30218,
#30219,#30220,#30221,#30222,#30223,#30224,#30225,#30226,#30227,#30228,#30229,
#30230,#30231,#30232,#30233,#30234,#30235,#30236,#30237,#30238,#30239,#30240,
#30241,#30242,#30243,#30244,#30245,#30246,#30247,#30248,#30249,#30250,#30251,
#30252,#30253,#30254,#30255,#30256,#30257,#30258,#30259,#30260,#30261,#30262,
#30263,#30264,#30265,#30266,#30267,#30268,#30269,#30270,#30271,#30272,#30273,
#30274,#30275,#30276,#30277,#30278,#30279,#30280,#30281,#30282,#30283,#30284,
#30285,#30286,#30287,#30288,#30289,#30290,#30291,#30292,#30293,#30294,#30295,
#30296,#30297,#30298,#30299,#30300,#30301,#30302,#30303,#30304,#30305,#30306,
#30307,#30308,#30309,#30310,#30311,#30312,#30313,#30314,#30315,#30316,#30317,
#30318,#30319,#30320,#30321,#30322,#30323,#30324,#30325,#30326,#30327,#30328,
#30329,#30330,#30331,#30332,#30333,#30334,#30335,#30336,#30337,#30338,#30339,
#30340,#30341,#30342,#30343,#30344,#30345,#30346,#30347,#30348,#30349,#30350,
#30351,#30352,#30353,#30354,#30355,#30356,#30357,#30358,#30359,#30360,#30361,
#30362,#30363,#30364,#30365,#30366,#30367,#30368,#30369,#30370,#30371,#30372,
#30373,#30374,#30375,#30376),.UNSPECIFIED.,.F.,.F.,(4,3,3,3,3,3,3,3,3,3,
3,3,3,3,3,3,3,3,3,3,3,3,3,3,3,3,3,3,3,3,3,3,3,3,3,3,3,3,3,3,3,3,3,3,3,3,
3,3,3,3,3,3,3,3,3,3,3,3,3,3,3,3,3,3,3,3,3,3,3,3,3,3,3,3,3,3,4),(486.946861306547,
487.029354407844,487.111760521916,487.194100759532,487.276402556392,487.358686132498,
487.440970475139,487.523274569938,487.605664188744,487.688101102786,487.770659626157,
487.818003922832,487.901750655534,487.98539433255,488.068955076616,488.152452938574,
488.235915439136,488.319360574628,488.402806409471,488.48627100471,488.569824190132,
488.653422023704,488.737153586566,488.816987425032,488.900734157734,488.98437783475,
489.067938578817,489.151436440773,489.234898941336,489.318344076828,489.401789911671,
489.485254506909,489.568807692331,489.652405525903,489.736137088765,489.815970927231,
489.899717659933,489.983361336949,490.066922081015,490.150419942972,490.233882443535,
490.317327579027,490.40077341387,490.484238009108,490.567791194529,490.651389028102,
490.735120590964,490.81495442943,490.898701162132,490.982344839147,491.065905583214,
491.14940344517,491.232865945733,491.316311081225,491.399756916068,491.483221511306,
491.566774696728,491.6503725303,491.734104093162,491.813937931629,491.897684664331,
491.981328341347,492.064889085414,492.148386947371,492.231849447933,492.315294583426,
492.398740418269,492.482205013506,492.565758198928,492.649356032501,492.733087595363,
492.812921433828,492.905016102355,492.99675842005,493.088275305412,493.179434747582,
493.230046613438),.UNSPECIFIED.);
#339=B_SPLINE_CURVE_WITH_KNOTS('',3,(#30378,#30379,#30380,#30381,#30382,
#30383,#30384,#30385,#30386,#30387,#30388,#30389,#30390,#30391,#30392,#30393,
#30394,#30395,#30396,#30397,#30398,#30399,#30400,#30401,#30402,#30403,#30404,
#30405,#30406,#30407,#30408,#30409,#30410,#30411,#30412,#30413,#30414,#30415,
#30416,#30417,#30418,#30419,#30420,#30421,#30422,#30423,#30424,#30425,#30426,
#30427,#30428,#30429,#30430,#30431,#30432,#30433,#30434,#30435,#30436,#30437,
#30438,#30439,#30440,#30441,#30442,#30443,#30444,#30445,#30446,#30447,#30448,
#30449,#30450,#30451,#30452,#30453,#30454,#30455,#30456,#30457,#30458,#30459,
#30460,#30461,#30462,#30463,#30464,#30465,#30466,#30467,#30468,#30469,#30470,
#30471,#30472,#30473,#30474,#30475,#30476,#30477,#30478,#30479,#30480,#30481,
#30482,#30483,#30484,#30485,#30486,#30487,#30488,#30489,#30490,#30491,#30492,
#30493,#30494,#30495,#30496,#30497,#30498,#30499,#30500,#30501,#30502,#30503,
#30504,#30505,#30506,#30507,#30508,#30509,#30510,#30511,#30512,#30513,#30514,
#30515,#30516,#30517,#30518,#30519,#30520,#30521,#30522,#30523,#30524,#30525,
#30526,#30527,#30528,#30529,#30530,#30531,#30532,#30533,#30534,#30535,#30536,
#30537,#30538,#30539,#30540,#30541,#30542,#30543,#30544,#30545,#30546,#30547,
#30548,#30549,#30550,#30551,#30552,#30553,#30554,#30555,#30556,#30557,#30558,
#30559,#30560,#30561,#30562,#30563,#30564,#30565,#30566,#30567,#30568,#30569,
#30570,#30571,#30572,#30573,#30574,#30575,#30576,#30577,#30578,#30579,#30580,
#30581,#30582,#30583,#30584,#30585,#30586,#30587,#30588,#30589,#30590,#30591,
#30592,#30593,#30594,#30595,#30596,#30597,#30598,#30599,#30600,#30601,#30602,
#30603),.UNSPECIFIED.,.F.,.F.,(4,3,3,3,3,3,3,3,3,3,3,3,3,3,3,3,3,3,3,3,
3,3,3,3,3,3,3,3,3,3,3,3,3,3,3,3,3,3,3,3,3,3,3,3,3,3,3,3,3,3,3,3,3,3,3,3,
3,3,3,3,3,3,3,3,3,3,3,3,3,3,3,3,3,3,3,4),(480.663675999239,480.799184202979,
480.825119407438,480.90886614014,480.992509817156,481.076070561222,481.159568423179,
481.243030923742,481.326476059234,481.409921894077,481.493386489315,481.576939674737,
481.66053750831,481.744269071172,481.824102909637,481.907849642339,481.991493319355,
482.075054063422,482.158551925378,482.242014425941,482.325459561433,482.408905396276,
482.492369991514,482.575923176936,482.659521010509,482.743252573371,482.823086411837,
482.906833144539,482.990476821555,483.074037565621,483.157535427578,483.240997928141,
483.324443063633,483.407888898476,483.491353493714,483.574906679136,483.658504512709,
483.742236075571,483.822069914036,483.905816646738,483.989460323754,484.07302106782,
484.156518929777,484.239981430339,484.323426565832,484.406872400674,484.490336995912,
484.573890181334,484.657488014907,484.741219577769,484.821053416235,484.904800148937,
484.988443825953,485.072004570019,485.155502431976,485.238964932539,485.322410068031,
485.405855902874,485.489320498112,485.572873683533,485.656471517106,485.740203079968,
485.820036918434,485.903783651136,485.987427328152,486.070988072219,486.154485934175,
486.237948434738,486.32139357023,486.404839405073,486.488304000312,486.571857185734,
486.655455019306,486.739186582168,486.819020420633,486.946861306418),
 .UNSPECIFIED.);
#340=B_SPLINE_CURVE_WITH_KNOTS('',3,(#30605,#30606,#30607,#30608,#30609,
#30610,#30611,#30612,#30613,#30614,#30615,#30616,#30617,#30618,#30619,#30620,
#30621,#30622,#30623,#30624,#30625,#30626,#30627,#30628,#30629,#30630,#30631,
#30632,#30633,#30634,#30635,#30636,#30637,#30638,#30639,#30640,#30641,#30642,
#30643,#30644,#30645,#30646,#30647,#30648,#30649,#30650,#30651,#30652,#30653,
#30654,#30655,#30656,#30657,#30658,#30659,#30660,#30661,#30662,#30663,#30664,
#30665,#30666,#30667,#30668,#30669,#30670,#30671,#30672,#30673,#30674,#30675,
#30676,#30677,#30678,#30679,#30680,#30681,#30682,#30683,#30684,#30685,#30686,
#30687,#30688,#30689,#30690,#30691,#30692,#30693,#30694,#30695,#30696,#30697,
#30698,#30699,#30700,#30701,#30702,#30703,#30704,#30705,#30706,#30707,#30708,
#30709,#30710,#30711,#30712,#30713,#30714,#30715,#30716,#30717,#30718,#30719,
#30720,#30721,#30722,#30723,#30724,#30725,#30726,#30727,#30728,#30729,#30730,
#30731,#30732,#30733,#30734,#30735,#30736,#30737,#30738,#30739,#30740,#30741,
#30742,#30743,#30744,#30745,#30746,#30747,#30748,#30749,#30750,#30751,#30752,
#30753,#30754,#30755,#30756,#30757,#30758,#30759,#30760,#30761,#30762,#30763,
#30764,#30765,#30766,#30767,#30768,#30769,#30770,#30771,#30772,#30773,#30774,
#30775,#30776,#30777,#30778,#30779,#30780,#30781,#30782,#30783,#30784,#30785,
#30786,#30787,#30788,#30789,#30790,#30791,#30792,#30793,#30794,#30795,#30796,
#30797,#30798,#30799,#30800,#30801,#30802,#30803,#30804,#30805,#30806,#30807,
#30808,#30809,#30810,#30811,#30812,#30813,#30814,#30815,#30816,#30817,#30818,
#30819,#30820,#30821,#30822,#30823,#30824,#30825,#30826,#30827,#30828,#30829,
#30830,#30831,#30832,#30833),.UNSPECIFIED.,.F.,.F.,(4,3,3,3,3,3,3,3,3,3,
3,3,3,3,3,3,3,3,3,3,3,3,3,3,3,3,3,3,3,3,3,3,3,3,3,3,3,3,3,3,3,3,3,3,3,3,
3,3,3,3,3,3,3,3,3,3,3,3,3,3,3,3,3,3,3,3,3,3,3,3,3,3,3,3,3,3,4),(474.38049069216,
474.469894373571,474.560225378739,474.650111625864,474.740665010053,474.831218394243,
474.914965126945,474.998608803961,475.082169548027,475.165667409984,475.249129910547,
475.332575046039,475.416020880882,475.499485476121,475.583038661543,475.666636495115,
475.750368057977,475.830201896442,475.913948629144,475.99759230616,476.081153050227,
476.164650912183,476.248113412746,476.331558548238,476.415004383081,476.49846897832,
476.582022163741,476.665619997314,476.749351560176,476.829185398642,476.912932131344,
476.99657580836,477.080136552426,477.163634414383,477.247096914946,477.330542050438,
477.413987885281,477.497452480519,477.58100566594,477.664603499513,477.748335062375,
477.828168900841,477.911915633543,477.995559310559,478.079120054625,478.162617916582,
478.246080417144,478.329525552637,478.412971387479,478.496435982717,478.579989168139,
478.663587001712,478.747318564574,478.82715240304,478.910899135742,478.994542812758,
479.078103556824,479.161601418781,479.245063919344,479.328509054836,479.411954889679,
479.495419484917,479.578972670339,479.662570503911,479.746302066773,479.826135905239,
479.908635321382,479.991032287064,480.075112751061,480.157365169424,480.239585411973,
480.321792518385,480.407263388548,480.489535156797,480.571843341417,480.654237625803,
480.663675999038),.UNSPECIFIED.);
#341=B_SPLINE_CURVE_WITH_KNOTS('',3,(#30835,#30836,#30837,#30838,#30839,
#30840,#30841,#30842,#30843,#30844,#30845,#30846,#30847,#30848,#30849,#30850,
#30851,#30852,#30853,#30854,#30855,#30856,#30857,#30858,#30859,#30860,#30861,
#30862,#30863,#30864,#30865,#30866,#30867,#30868,#30869,#30870,#30871,#30872,
#30873,#30874,#30875,#30876,#30877,#30878,#30879,#30880,#30881,#30882,#30883,
#30884,#30885,#30886,#30887,#30888,#30889,#30890,#30891,#30892,#30893,#30894,
#30895,#30896,#30897,#30898,#30899,#30900,#30901,#30902,#30903,#30904,#30905,
#30906,#30907,#30908,#30909,#30910,#30911,#30912,#30913,#30914,#30915,#30916,
#30917,#30918,#30919,#30920,#30921,#30922,#30923,#30924,#30925,#30926,#30927,
#30928,#30929,#30930,#30931,#30932,#30933,#30934,#30935,#30936,#30937,#30938,
#30939,#30940,#30941,#30942,#30943,#30944,#30945,#30946,#30947,#30948,#30949,
#30950,#30951,#30952,#30953,#30954,#30955,#30956,#30957,#30958,#30959,#30960,
#30961,#30962,#30963,#30964,#30965,#30966,#30967,#30968,#30969,#30970,#30971,
#30972,#30973,#30974,#30975,#30976,#30977,#30978,#30979,#30980,#30981,#30982,
#30983,#30984,#30985,#30986,#30987,#30988,#30989,#30990,#30991,#30992,#30993,
#30994,#30995,#30996,#30997,#30998,#30999,#31000,#31001,#31002,#31003,#31004,
#31005,#31006,#31007,#31008,#31009,#31010,#31011,#31012,#31013,#31014,#31015,
#31016,#31017,#31018,#31019,#31020,#31021,#31022,#31023,#31024,#31025,#31026,
#31027,#31028,#31029,#31030,#31031,#31032,#31033,#31034,#31035,#31036,#31037,
#31038,#31039,#31040,#31041,#31042,#31043,#31044,#31045,#31046,#31047,#31048,
#31049,#31050,#31051,#31052,#31053,#31054,#31055,#31056,#31057,#31058,#31059,
#31060,#31061,#31062,#31063),.UNSPECIFIED.,.F.,.F.,(4,3,3,3,3,3,3,3,3,3,
3,3,3,3,3,3,3,3,3,3,3,3,3,3,3,3,3,3,3,3,3,3,3,3,3,3,3,3,3,3,3,3,3,3,3,3,
3,3,3,3,3,3,3,3,3,3,3,3,3,3,3,3,3,3,3,3,3,3,3,3,3,3,3,3,3,3,4),(468.09730538488,
468.179935268047,468.262520399752,468.34508270027,468.427640970441,468.510214005244,
468.592871668108,468.675571756588,468.758404179363,468.837317381048,468.92106411375,
469.004707790766,469.088268534832,469.171766396789,469.255228897352,469.338674032844,
469.422119867687,469.505584462925,469.589137648347,469.672735481919,469.756467044781,
469.836300883247,469.920047615949,470.003691292965,470.087252037032,470.170749898988,
470.254212399551,470.337657535043,470.421103369886,470.504567965124,470.588121150545,
470.671718984118,470.75545054698,470.835284385447,470.919031118149,471.002674795165,
471.086235539232,471.169733401188,471.253195901751,471.336641037243,471.420086872086,
471.503551467325,471.587104652747,471.670702486319,471.754434049181,471.834267887646,
471.918014620348,472.001658297364,472.08521904143,472.168716903387,472.252179403949,
472.335624539442,472.419070374284,472.502534969522,472.586088154944,472.669685988517,
472.753417551379,472.833251389845,472.916998122547,473.000641799562,473.084202543629,
473.167700405586,473.251162906148,473.33460804164,473.418053876483,473.501518471721,
473.585071657143,473.668669490715,473.752401053577,473.832234892044,473.918590158789,
474.004817581131,474.090930999263,474.17691500735,474.262822406883,474.348650729396,
474.380490692059),.UNSPECIFIED.);
#342=B_SPLINE_CURVE_WITH_KNOTS('',3,(#31065,#31066,#31067,#31068,#31069,
#31070,#31071,#31072,#31073,#31074,#31075),.UNSPECIFIED.,.F.,.F.,(4,1,1,
1,1,1,1,1,4),(461.8141200777,461.844432865654,462.843416367853,463.842399870052,
464.841383372252,465.840366874451,466.83935037665,467.838333878849,468.097302840225),
 .UNSPECIFIED.);
#343=B_SPLINE_CURVE_WITH_KNOTS('',3,(#31077,#31078,#31079,#31080,#31081,
#31082,#31083,#31084,#31085,#31086,#31087,#31088,#31089,#31090,#31091,#31092,
#31093,#31094,#31095,#31096,#31097,#31098,#31099,#31100,#31101,#31102,#31103,
#31104,#31105,#31106,#31107,#31108,#31109,#31110,#31111,#31112,#31113,#31114,
#31115,#31116,#31117,#31118,#31119,#31120,#31121,#31122,#31123,#31124,#31125,
#31126,#31127,#31128,#31129,#31130,#31131,#31132,#31133,#31134,#31135,#31136,
#31137,#31138,#31139,#31140,#31141,#31142,#31143,#31144,#31145,#31146,#31147,
#31148,#31149,#31150,#31151,#31152,#31153,#31154,#31155,#31156,#31157,#31158,
#31159,#31160,#31161,#31162,#31163,#31164,#31165,#31166,#31167,#31168,#31169,
#31170,#31171,#31172,#31173,#31174,#31175,#31176,#31177,#31178,#31179,#31180,
#31181,#31182,#31183,#31184,#31185,#31186,#31187,#31188,#31189,#31190,#31191,
#31192,#31193,#31194,#31195,#31196,#31197,#31198,#31199,#31200,#31201,#31202,
#31203,#31204,#31205,#31206,#31207,#31208,#31209,#31210,#31211,#31212,#31213,
#31214,#31215,#31216,#31217,#31218,#31219,#31220,#31221,#31222,#31223,#31224,
#31225,#31226,#31227,#31228,#31229,#31230,#31231,#31232,#31233,#31234,#31235,
#31236,#31237,#31238,#31239,#31240,#31241,#31242,#31243,#31244,#31245,#31246,
#31247,#31248,#31249,#31250,#31251,#31252,#31253,#31254,#31255,#31256,#31257,
#31258,#31259,#31260,#31261,#31262,#31263,#31264,#31265,#31266,#31267,#31268,
#31269,#31270,#31271,#31272,#31273,#31274,#31275,#31276,#31277,#31278,#31279,
#31280,#31281,#31282,#31283,#31284,#31285,#31286,#31287,#31288,#31289,#31290,
#31291,#31292,#31293,#31294,#31295,#31296,#31297,#31298,#31299,#31300,#31301,
#31302,#31303,#31304,#31305),.UNSPECIFIED.,.F.,.F.,(4,3,3,3,3,3,3,3,3,3,
3,3,3,3,3,3,3,3,3,3,3,3,3,3,3,3,3,3,3,3,3,3,3,3,3,3,3,3,3,3,3,3,3,3,3,3,
3,3,3,3,3,3,3,3,3,3,3,3,3,3,3,3,3,3,3,3,3,3,3,3,3,3,3,3,3,3,4),(455.530934770694,
455.629412302043,455.728568331284,455.828470220712,455.850531852459,455.934278585161,
456.017922262177,456.101483006244,456.184980868201,456.268443368763,456.351888504256,
456.435334339098,456.518798934337,456.602352119759,456.685949953331,456.769681516193,
456.849515354658,456.93326208736,457.016905764376,457.100466508443,457.183964370399,
457.267426870962,457.350872006454,457.434317841297,457.517782436535,457.601335621957,
457.68493345553,457.768665018392,457.848498856858,457.93224558956,458.015889266576,
458.099450010642,458.182947872599,458.266410373162,458.349855508654,458.433301343497,
458.516765938735,458.600319124157,458.683916957729,458.767648520591,458.847482359057,
458.931229091759,459.014872768775,459.098433512841,459.181931374798,459.265393875361,
459.348839010853,459.432284845696,459.515749440934,459.599302626355,459.682900459928,
459.76663202279,459.846465861256,459.930212593958,460.013856270974,460.09741701504,
460.180914876997,460.264377377559,460.347822513052,460.431268347895,460.514732943133,
460.598286128554,460.681883962127,460.765615524989,460.845449363455,460.92877944253,
461.012006735704,461.095151789752,461.178235075274,461.261284625204,461.344318559843,
461.427355319168,461.510413341538,461.593559004726,461.676752316929,461.760069949751,
461.814119801522),.UNSPECIFIED.);
#344=B_SPLINE_CURVE_WITH_KNOTS('',3,(#31307,#31308,#31309,#31310,#31311,
#31312,#31313,#31314,#31315,#31316,#31317,#31318,#31319,#31320,#31321,#31322,
#31323,#31324,#31325,#31326,#31327,#31328,#31329,#31330,#31331,#31332,#31333,
#31334,#31335,#31336,#31337,#31338,#31339,#31340,#31341,#31342,#31343,#31344,
#31345,#31346,#31347,#31348,#31349,#31350,#31351,#31352,#31353,#31354,#31355,
#31356,#31357,#31358,#31359,#31360,#31361,#31362,#31363,#31364,#31365,#31366,
#31367,#31368,#31369,#31370,#31371,#31372,#31373,#31374,#31375,#31376,#31377,
#31378,#31379,#31380,#31381,#31382,#31383,#31384,#31385,#31386,#31387,#31388,
#31389,#31390,#31391,#31392,#31393,#31394,#31395,#31396,#31397,#31398,#31399,
#31400,#31401,#31402,#31403,#31404,#31405,#31406,#31407,#31408,#31409,#31410,
#31411,#31412,#31413,#31414,#31415,#31416,#31417,#31418,#31419,#31420,#31421,
#31422,#31423,#31424,#31425,#31426,#31427,#31428,#31429,#31430,#31431,#31432,
#31433,#31434,#31435,#31436,#31437,#31438,#31439,#31440,#31441,#31442,#31443,
#31444,#31445,#31446,#31447,#31448,#31449,#31450,#31451,#31452,#31453,#31454,
#31455,#31456,#31457,#31458,#31459,#31460,#31461,#31462,#31463,#31464,#31465,
#31466,#31467,#31468,#31469,#31470,#31471,#31472,#31473,#31474,#31475,#31476,
#31477,#31478,#31479,#31480,#31481,#31482,#31483,#31484,#31485,#31486,#31487,
#31488,#31489,#31490,#31491,#31492,#31493,#31494,#31495,#31496,#31497,#31498,
#31499,#31500,#31501,#31502,#31503,#31504,#31505,#31506,#31507,#31508,#31509,
#31510,#31511,#31512,#31513,#31514,#31515,#31516,#31517,#31518,#31519,#31520,
#31521,#31522,#31523,#31524,#31525,#31526,#31527,#31528,#31529,#31530,#31531,
#31532,#31533,#31534,#31535,#31536,#31537,#31538),.UNSPECIFIED.,.F.,.F.,
(4,3,3,3,3,3,3,3,3,3,3,3,3,3,3,3,3,3,3,3,3,3,3,3,3,3,3,3,3,3,3,3,3,3,3,
3,3,3,3,3,3,3,3,3,3,3,3,3,3,3,3,3,3,3,3,3,3,3,3,3,3,3,3,3,3,3,3,3,3,3,3,
3,3,3,3,3,3,4),(449.247749463341,449.332121367645,449.416509550338,449.500930709019,
449.585401559849,449.669989170282,449.75464620782,449.839434812469,449.856630839264,
449.940377571966,450.024021248982,450.107581993048,450.191079855005,450.274542355568,
450.35798749106,450.441433325903,450.524897921141,450.608451106563,450.692048940136,
450.775780502997,450.855614341463,450.939361074165,451.023004751181,451.106565495247,
451.190063357204,451.273525857767,451.356970993259,451.440416828102,451.52388142334,
451.607434608761,451.691032442334,451.774764005196,451.854597843663,451.938344576365,
452.021988253381,452.105548997447,452.189046859404,452.272509359966,452.355954495459,
452.439400330302,452.52286492554,452.606418110962,452.690015944534,452.773747507396,
452.853581345862,452.937328078564,453.02097175558,453.104532499646,453.188030361602,
453.271492862165,453.354937997657,453.438383832499,453.521848427737,453.605401613159,
453.688999446732,453.772731009594,453.852564848061,453.936311580763,454.019955257779,
454.103516001846,454.187013863803,454.270476364365,454.353921499858,454.4373673347,
454.520831929939,454.604385115361,454.687982948933,454.771714511795,454.85154835026,
454.936471652793,455.019865229954,455.103178641182,455.186430241413,455.27255637369,
455.355747822368,455.438931987459,455.522140523525,455.530934770521),
 .UNSPECIFIED.);
#345=B_SPLINE_CURVE_WITH_KNOTS('',3,(#31540,#31541,#31542,#31543,#31544,
#31545,#31546,#31547,#31548,#31549,#31550,#31551,#31552,#31553,#31554,#31555,
#31556,#31557,#31558,#31559,#31560,#31561,#31562,#31563,#31564,#31565,#31566,
#31567,#31568,#31569,#31570,#31571,#31572,#31573,#31574,#31575,#31576,#31577,
#31578,#31579,#31580,#31581,#31582,#31583,#31584,#31585,#31586,#31587,#31588,
#31589,#31590,#31591,#31592,#31593,#31594,#31595,#31596,#31597,#31598,#31599,
#31600,#31601,#31602,#31603,#31604,#31605,#31606,#31607,#31608,#31609,#31610,
#31611,#31612,#31613,#31614,#31615,#31616,#31617,#31618,#31619,#31620,#31621,
#31622,#31623,#31624,#31625,#31626,#31627,#31628,#31629,#31630,#31631,#31632,
#31633,#31634,#31635,#31636,#31637,#31638,#31639,#31640,#31641,#31642,#31643,
#31644,#31645,#31646,#31647,#31648,#31649,#31650,#31651,#31652,#31653,#31654,
#31655,#31656,#31657,#31658,#31659,#31660,#31661,#31662,#31663,#31664,#31665,
#31666,#31667,#31668,#31669,#31670,#31671,#31672,#31673,#31674,#31675,#31676,
#31677,#31678,#31679,#31680,#31681,#31682,#31683,#31684,#31685,#31686,#31687,
#31688,#31689,#31690,#31691,#31692,#31693,#31694,#31695,#31696,#31697,#31698,
#31699,#31700,#31701,#31702,#31703,#31704,#31705,#31706,#31707,#31708,#31709,
#31710,#31711,#31712,#31713,#31714,#31715,#31716,#31717,#31718,#31719,#31720,
#31721,#31722,#31723,#31724,#31725,#31726,#31727,#31728,#31729,#31730,#31731,
#31732,#31733,#31734,#31735,#31736,#31737,#31738,#31739,#31740,#31741,#31742,
#31743,#31744,#31745,#31746,#31747,#31748,#31749,#31750,#31751,#31752,#31753,
#31754,#31755,#31756,#31757,#31758,#31759,#31760,#31761,#31762,#31763,#31764,
#31765,#31766,#31767,#31768),.UNSPECIFIED.,.F.,.F.,(4,3,3,3,3,3,3,3,3,3,
3,3,3,3,3,3,3,3,3,3,3,3,3,3,3,3,3,3,3,3,3,3,3,3,3,3,3,3,3,3,3,3,3,3,3,3,
3,3,3,3,3,3,3,3,3,3,3,3,3,3,3,3,3,3,3,3,3,3,3,3,3,3,3,3,3,3,4),(442.964564156297,
443.047208221643,443.129759939605,443.212240350628,443.294675061561,443.377086506837,
443.459493597428,443.541915238339,443.624420188387,443.706967604258,443.789644235641,
443.862729826069,443.946476558771,444.030120235787,444.113680979854,444.19717884181,
444.280641342373,444.364086477865,444.447532312708,444.530996907947,444.614550093369,
444.698147926941,444.781879489803,444.861713328268,444.94546006097,445.029103737986,
445.112664482052,445.19616234401,445.279624844572,445.363069980065,445.446515814908,
445.529980410146,445.613533595568,445.697131429141,445.780862992003,445.860696830468,
445.94444356317,446.028087240186,446.111647984252,446.195145846209,446.278608346771,
446.362053482264,446.445499317107,446.528963912345,446.612517097766,446.696114931339,
446.779846494201,446.859680332667,446.943427065369,447.027070742385,447.110631486451,
447.194129348408,447.27759184897,447.361036984462,447.444482819305,447.527947414543,
447.611500599965,447.695098433538,447.7788299964,447.858663834866,447.942410567568,
448.026054244584,448.10961498865,448.193112850607,448.276575351169,448.360020486662,
448.443466321505,448.526930916743,448.610484102165,448.694081935738,448.7778134986,
448.857647337065,448.955172868587,449.048592193972,449.141721584224,449.234411531842,
449.247749463153),.UNSPECIFIED.);
#346=B_SPLINE_CURVE_WITH_KNOTS('',3,(#31770,#31771,#31772,#31773,#31774,
#31775,#31776,#31777,#31778,#31779,#31780,#31781,#31782,#31783,#31784,#31785,
#31786,#31787,#31788,#31789,#31790,#31791,#31792,#31793,#31794,#31795,#31796,
#31797,#31798,#31799,#31800,#31801,#31802,#31803,#31804,#31805,#31806,#31807,
#31808,#31809,#31810,#31811,#31812,#31813,#31814,#31815,#31816,#31817,#31818,
#31819,#31820,#31821,#31822,#31823,#31824,#31825,#31826,#31827,#31828,#31829,
#31830,#31831,#31832,#31833,#31834,#31835,#31836,#31837,#31838,#31839,#31840,
#31841,#31842,#31843,#31844,#31845,#31846,#31847,#31848,#31849,#31850,#31851,
#31852,#31853,#31854,#31855,#31856,#31857,#31858,#31859,#31860,#31861,#31862,
#31863,#31864,#31865,#31866,#31867,#31868,#31869,#31870,#31871,#31872,#31873,
#31874,#31875,#31876,#31877,#31878,#31879,#31880,#31881,#31882,#31883,#31884,
#31885,#31886,#31887,#31888,#31889,#31890,#31891,#31892,#31893,#31894,#31895,
#31896,#31897,#31898,#31899,#31900,#31901,#31902,#31903,#31904,#31905,#31906,
#31907,#31908,#31909,#31910,#31911,#31912,#31913,#31914,#31915,#31916,#31917,
#31918,#31919,#31920,#31921,#31922,#31923,#31924,#31925,#31926,#31927,#31928,
#31929,#31930,#31931,#31932,#31933,#31934,#31935,#31936,#31937,#31938,#31939,
#31940,#31941,#31942,#31943,#31944,#31945,#31946,#31947,#31948,#31949,#31950,
#31951,#31952,#31953,#31954,#31955,#31956,#31957,#31958,#31959,#31960,#31961,
#31962,#31963,#31964,#31965,#31966,#31967,#31968,#31969,#31970,#31971,#31972,
#31973,#31974,#31975,#31976,#31977,#31978,#31979,#31980,#31981,#31982,#31983,
#31984,#31985,#31986,#31987,#31988,#31989,#31990,#31991,#31992,#31993,#31994,
#31995),.UNSPECIFIED.,.F.,.F.,(4,3,3,3,3,3,3,3,3,3,3,3,3,3,3,3,3,3,3,3,
3,3,3,3,3,3,3,3,3,3,3,3,3,3,3,3,3,3,3,3,3,3,3,3,3,3,3,3,3,3,3,3,3,3,3,3,
3,3,3,3,3,3,3,3,3,3,3,3,3,3,3,3,3,3,3,4),(436.681378848982,436.805218179798,
436.869845310675,436.953592043377,437.037235720393,437.12079646446,437.204294326416,
437.287756826979,437.371201962471,437.454647797314,437.538112392552,437.621665577974,
437.705263411547,437.788994974409,437.868828812874,437.952575545576,438.036219222592,
438.119779966658,438.203277828615,438.286740329178,438.37018546467,438.453631299513,
438.537095894751,438.620649080173,438.704246913745,438.787978476607,438.867812315073,
438.951559047775,439.035202724791,439.118763468857,439.202261330814,439.285723831377,
439.369168966869,439.452614801712,439.53607939695,439.619632582372,439.703230415945,
439.786961978807,439.866795817273,439.950542549975,440.034186226991,440.117746971057,
440.201244833014,440.284707333577,440.368152469069,440.451598303912,440.53506289915,
440.618616084572,440.702213918145,440.785945481007,440.865779319472,440.949526052174,
441.03316972919,441.116730473256,441.200228335213,441.283690835775,441.367135971268,
441.450581806111,441.534046401348,441.61759958677,441.701197420343,441.784928983205,
441.864762821671,441.948509554373,442.032153231388,442.115713975455,442.199211837411,
442.282674337974,442.366119473466,442.449565308309,442.533029903547,442.616583088969,
442.700180922541,442.783912485403,442.86374632387,442.964564156162),
 .UNSPECIFIED.);
#347=B_SPLINE_CURVE_WITH_KNOTS('',3,(#31997,#31998,#31999,#32000,#32001,
#32002,#32003,#32004,#32005,#32006,#32007,#32008,#32009,#32010,#32011,#32012,
#32013,#32014,#32015,#32016,#32017,#32018,#32019,#32020,#32021,#32022,#32023,
#32024,#32025,#32026,#32027,#32028,#32029,#32030,#32031,#32032,#32033,#32034,
#32035,#32036,#32037,#32038,#32039,#32040,#32041,#32042,#32043,#32044,#32045,
#32046,#32047,#32048,#32049,#32050,#32051,#32052,#32053,#32054,#32055,#32056,
#32057,#32058,#32059,#32060,#32061,#32062,#32063,#32064,#32065,#32066,#32067,
#32068,#32069,#32070,#32071,#32072,#32073,#32074,#32075,#32076,#32077,#32078,
#32079,#32080,#32081,#32082,#32083,#32084,#32085,#32086,#32087,#32088,#32089,
#32090,#32091,#32092,#32093,#32094,#32095,#32096,#32097,#32098,#32099,#32100,
#32101,#32102,#32103,#32104,#32105,#32106,#32107,#32108,#32109,#32110,#32111,
#32112,#32113,#32114,#32115,#32116,#32117,#32118,#32119,#32120,#32121,#32122,
#32123,#32124,#32125,#32126,#32127,#32128,#32129,#32130,#32131,#32132,#32133,
#32134,#32135,#32136,#32137,#32138,#32139,#32140,#32141,#32142,#32143,#32144,
#32145,#32146,#32147,#32148,#32149,#32150,#32151,#32152,#32153,#32154,#32155,
#32156,#32157,#32158,#32159,#32160,#32161,#32162,#32163,#32164,#32165,#32166,
#32167,#32168,#32169,#32170,#32171,#32172,#32173,#32174,#32175,#32176,#32177,
#32178,#32179,#32180,#32181,#32182,#32183,#32184,#32185,#32186,#32187,#32188,
#32189,#32190,#32191,#32192,#32193,#32194,#32195,#32196,#32197,#32198,#32199,
#32200,#32201,#32202,#32203,#32204,#32205,#32206,#32207,#32208,#32209,#32210,
#32211,#32212,#32213,#32214,#32215,#32216,#32217,#32218,#32219,#32220,#32221,
#32222,#32223,#32224,#32225),.UNSPECIFIED.,.F.,.F.,(4,3,3,3,3,3,3,3,3,3,
3,3,3,3,3,3,3,3,3,3,3,3,3,3,3,3,3,3,3,3,3,3,3,3,3,3,3,3,3,3,3,3,3,3,3,3,
3,3,3,3,3,3,3,3,3,3,3,3,3,3,3,3,3,3,3,3,3,3,3,3,3,3,3,3,3,3,4),(430.398193541985,
430.486432197338,430.574817646461,430.66344055964,430.752192696424,430.84115178814,
430.87594429748,430.959691030182,431.043334707198,431.126895451264,431.210393313221,
431.293855813784,431.377300949276,431.460746784119,431.544211379357,431.627764564778,
431.711362398351,431.795093961213,431.874927799679,431.958674532381,432.042318209397,
432.125878953464,432.20937681542,432.292839315983,432.376284451475,432.459730286318,
432.543194881556,432.626748066978,432.710345900551,432.794077463413,432.873911301878,
432.95765803458,433.041301711596,433.124862455662,433.208360317619,433.291822818182,
433.375267953674,433.458713788517,433.542178383755,433.625731569177,433.709329402749,
433.793060965611,433.872894804078,433.95664153678,434.040285213796,434.123845957862,
434.207343819819,434.290806320382,434.374251455874,434.457697290717,434.541161885955,
434.624715071377,434.70831290495,434.792044467812,434.871878306277,434.955625038979,
435.039268715995,435.122829460061,435.206327322018,435.289789822581,435.373234958073,
435.456680792916,435.540145388154,435.623698573575,435.707296407148,435.79102797001,
435.870861808476,435.953377350882,436.035790000206,436.118109323625,436.200376371044,
436.282610205523,436.364829859162,436.447087832864,436.529363788295,436.611727654349,
436.68137884885),.UNSPECIFIED.);
#348=B_SPLINE_CURVE_WITH_KNOTS('',3,(#32227,#32228,#32229,#32230,#32231,
#32232,#32233,#32234,#32235,#32236,#32237,#32238,#32239,#32240,#32241,#32242,
#32243,#32244,#32245,#32246,#32247,#32248,#32249,#32250,#32251,#32252,#32253,
#32254,#32255,#32256,#32257,#32258,#32259,#32260,#32261,#32262,#32263,#32264,
#32265,#32266,#32267,#32268,#32269,#32270,#32271,#32272,#32273,#32274,#32275,
#32276,#32277,#32278,#32279,#32280,#32281,#32282,#32283,#32284,#32285,#32286,
#32287,#32288,#32289,#32290,#32291,#32292,#32293,#32294,#32295,#32296,#32297,
#32298,#32299,#32300,#32301,#32302,#32303,#32304,#32305,#32306,#32307,#32308,
#32309,#32310,#32311,#32312,#32313,#32314,#32315,#32316,#32317,#32318,#32319,
#32320,#32321,#32322,#32323,#32324,#32325,#32326,#32327,#32328,#32329,#32330,
#32331,#32332,#32333,#32334,#32335,#32336,#32337,#32338,#32339,#32340,#32341,
#32342,#32343,#32344,#32345,#32346,#32347,#32348,#32349,#32350,#32351,#32352,
#32353,#32354,#32355,#32356,#32357,#32358,#32359,#32360,#32361,#32362,#32363,
#32364,#32365,#32366,#32367,#32368,#32369,#32370,#32371,#32372,#32373,#32374,
#32375,#32376,#32377,#32378,#32379,#32380,#32381,#32382,#32383,#32384,#32385,
#32386,#32387,#32388,#32389,#32390,#32391,#32392,#32393,#32394,#32395,#32396,
#32397,#32398,#32399,#32400,#32401,#32402,#32403,#32404,#32405,#32406,#32407,
#32408,#32409,#32410,#32411,#32412,#32413,#32414,#32415,#32416,#32417,#32418,
#32419,#32420,#32421,#32422,#32423,#32424,#32425,#32426,#32427,#32428,#32429,
#32430,#32431,#32432,#32433,#32434,#32435,#32436,#32437,#32438,#32439,#32440,
#32441,#32442,#32443,#32444,#32445,#32446,#32447,#32448,#32449,#32450,#32451,
#32452,#32453,#32454,#32455),.UNSPECIFIED.,.F.,.F.,(4,3,3,3,3,3,3,3,3,3,
3,3,3,3,3,3,3,3,3,3,3,3,3,3,3,3,3,3,3,3,3,3,3,3,3,3,3,3,3,3,3,3,3,3,3,3,
3,3,3,3,3,3,3,3,3,3,3,3,3,3,3,3,3,3,3,3,3,3,3,3,3,3,3,3,3,3,4),(424.1150082348,
424.197489161053,424.283058426457,424.365449984924,424.447830114361,424.530217734788,
424.612631769645,424.695135102409,424.777691588687,424.86036356663,424.882043284285,
424.965790016987,425.049433694003,425.132994438069,425.216492300025,425.299954800588,
425.38339993608,425.466845770923,425.550310366161,425.633863551583,425.717461385156,
425.801192948018,425.881026786484,425.964773519186,426.048417196202,426.131977940269,
426.215475802226,426.298938302788,426.382383438281,426.465829273124,426.549293868362,
426.632847053784,426.716444887356,426.800176450218,426.880010288683,426.963757021385,
427.047400698401,427.130961442467,427.214459304424,427.297921804987,427.381366940479,
427.464812775322,427.54827737056,427.631830555981,427.715428389554,427.799159952416,
427.878993790883,427.962740523585,428.046384200601,428.129944944667,428.213442806624,
428.296905307187,428.380350442679,428.463796277522,428.54726087276,428.630814058182,
428.714411891755,428.798143454617,428.877977293082,428.961724025784,429.0453677028,
429.128928446866,429.212426308823,429.295888809386,429.379333944878,429.462779779721,
429.546244374959,429.629797560381,429.713395393953,429.797126956815,429.876960795281,
429.96420706254,430.051313696243,430.138242590583,430.225067797765,430.311763821276,
430.398193541802),.UNSPECIFIED.);
#349=B_SPLINE_CURVE_WITH_KNOTS('',3,(#32457,#32458,#32459,#32460,#32461,
#32462,#32463,#32464,#32465,#32466,#32467,#32468,#32469,#32470,#32471,#32472,
#32473,#32474,#32475,#32476,#32477,#32478,#32479,#32480,#32481,#32482,#32483,
#32484,#32485,#32486,#32487,#32488,#32489,#32490,#32491,#32492,#32493,#32494,
#32495,#32496,#32497,#32498,#32499,#32500,#32501,#32502,#32503,#32504,#32505,
#32506,#32507,#32508,#32509,#32510,#32511,#32512,#32513,#32514,#32515,#32516,
#32517,#32518,#32519,#32520,#32521,#32522,#32523,#32524,#32525,#32526,#32527,
#32528,#32529,#32530,#32531,#32532,#32533,#32534,#32535,#32536,#32537,#32538,
#32539,#32540,#32541,#32542,#32543,#32544,#32545,#32546,#32547,#32548,#32549,
#32550,#32551,#32552,#32553,#32554,#32555,#32556,#32557,#32558,#32559,#32560,
#32561,#32562,#32563,#32564,#32565,#32566,#32567,#32568,#32569,#32570,#32571,
#32572,#32573,#32574,#32575,#32576,#32577,#32578,#32579,#32580,#32581,#32582,
#32583,#32584,#32585,#32586,#32587,#32588,#32589,#32590,#32591,#32592,#32593,
#32594,#32595,#32596,#32597,#32598,#32599,#32600,#32601,#32602,#32603,#32604,
#32605,#32606,#32607,#32608,#32609,#32610,#32611,#32612,#32613,#32614,#32615,
#32616,#32617,#32618,#32619,#32620,#32621,#32622,#32623,#32624,#32625,#32626,
#32627,#32628,#32629,#32630,#32631,#32632,#32633,#32634,#32635,#32636,#32637,
#32638,#32639,#32640,#32641,#32642,#32643,#32644,#32645,#32646,#32647,#32648,
#32649,#32650,#32651,#32652,#32653,#32654,#32655,#32656,#32657,#32658,#32659,
#32660,#32661,#32662,#32663,#32664,#32665,#32666,#32667,#32668,#32669,#32670,
#32671,#32672,#32673,#32674,#32675,#32676,#32677,#32678,#32679,#32680,#32681,
#32682),.UNSPECIFIED.,.F.,.F.,(4,3,3,3,3,3,3,3,3,3,3,3,3,3,3,3,3,3,3,3,
3,3,3,3,3,3,3,3,3,3,3,3,3,3,3,3,3,3,3,3,3,3,3,3,3,3,3,3,3,3,3,3,3,3,3,3,
3,3,3,3,3,3,3,3,3,3,3,3,3,3,3,3,3,3,3,4),(417.831822927443,417.889158768891,
417.972905501593,418.056549178609,418.140109922675,418.223607784632,418.307070285195,
418.390515420687,418.47396125553,418.557425850768,418.64097903619,418.724576869763,
418.808308432624,418.88814227109,418.971889003792,419.055532680808,419.139093424874,
419.222591286831,419.306053787393,419.389498922885,419.472944757728,419.556409352966,
419.639962538388,419.723560371961,419.807291934823,419.887125773289,419.970872505991,
420.054516183007,420.138076927073,420.22157478903,420.305037289593,420.388482425085,
420.471928259928,420.555392855166,420.638946040588,420.72254387416,420.806275437022,
420.886109275488,420.96985600819,421.053499685206,421.137060429273,421.220558291229,
421.304020791792,421.387465927284,421.470911762127,421.554376357365,421.637929542787,
421.72152737636,421.805258939222,421.885092777688,421.96883951039,422.052483187406,
422.136043931472,422.219541793429,422.303004293992,422.386449429484,422.469895264327,
422.553359859565,422.636913044987,422.72051087856,422.804242441422,422.884076279887,
422.967823012589,423.051466689605,423.135027433671,423.218525295628,423.30198779619,
423.385432931682,423.468878766525,423.552343361763,423.635896547185,423.719494380758,
423.803225943619,423.883059782086,423.999034008354,424.115008234623),
 .UNSPECIFIED.);
#350=B_SPLINE_CURVE_WITH_KNOTS('',3,(#32684,#32685,#32686,#32687,#32688,
#32689,#32690,#32691,#32692,#32693),.UNSPECIFIED.,.F.,.F.,(4,1,1,1,1,1,
1,4),(411.548645183548,411.895257755696,412.894241257895,413.893224760094,
414.892208262293,415.891191764493,416.890175266692,417.831815876483),
 .UNSPECIFIED.);
#351=B_SPLINE_CURVE_WITH_KNOTS('',3,(#32695,#32696,#32697,#32698,#32699,
#32700,#32701,#32702,#32703,#32704,#32705,#32706,#32707,#32708,#32709,#32710,
#32711,#32712,#32713,#32714,#32715,#32716,#32717,#32718,#32719,#32720,#32721,
#32722,#32723,#32724,#32725,#32726,#32727,#32728,#32729,#32730,#32731,#32732,
#32733,#32734,#32735,#32736,#32737,#32738,#32739,#32740,#32741,#32742,#32743,
#32744,#32745,#32746,#32747,#32748,#32749,#32750,#32751,#32752,#32753,#32754,
#32755,#32756,#32757,#32758,#32759,#32760,#32761,#32762,#32763,#32764,#32765,
#32766,#32767,#32768,#32769,#32770,#32771,#32772,#32773,#32774,#32775,#32776,
#32777,#32778,#32779,#32780,#32781,#32782,#32783,#32784,#32785,#32786,#32787,
#32788,#32789,#32790,#32791,#32792,#32793,#32794,#32795,#32796,#32797,#32798,
#32799,#32800,#32801,#32802,#32803,#32804,#32805,#32806,#32807,#32808,#32809,
#32810,#32811,#32812,#32813,#32814,#32815,#32816,#32817,#32818,#32819,#32820,
#32821,#32822,#32823,#32824,#32825,#32826,#32827,#32828,#32829,#32830,#32831,
#32832,#32833,#32834,#32835,#32836,#32837,#32838,#32839,#32840,#32841,#32842,
#32843,#32844,#32845,#32846,#32847,#32848,#32849,#32850,#32851,#32852,#32853,
#32854,#32855,#32856,#32857,#32858,#32859,#32860,#32861,#32862,#32863,#32864,
#32865,#32866,#32867,#32868,#32869,#32870,#32871,#32872,#32873,#32874,#32875,
#32876,#32877,#32878,#32879,#32880,#32881,#32882,#32883,#32884,#32885,#32886,
#32887,#32888,#32889,#32890,#32891,#32892,#32893,#32894,#32895,#32896,#32897,
#32898,#32899,#32900,#32901,#32902,#32903,#32904,#32905,#32906,#32907,#32908,
#32909,#32910,#32911,#32912,#32913,#32914,#32915,#32916,#32917,#32918,#32919,
#32920,#32921,#32922,#32923),.UNSPECIFIED.,.F.,.F.,(4,3,3,3,3,3,3,3,3,3,
3,3,3,3,3,3,3,3,3,3,3,3,3,3,3,3,3,3,3,3,3,3,3,3,3,3,3,3,3,3,3,3,3,3,3,3,
3,3,3,3,3,3,3,3,3,3,3,3,3,3,3,3,3,3,3,3,3,3,3,3,3,3,3,3,3,3,4),(405.265452313084,
405.34931675342,405.433182297519,405.517066410324,405.600986564986,405.685012608218,
405.769097414882,405.853317495139,405.901356742501,405.985103475203,406.068747152219,
406.152307896285,406.235805758242,406.319268258804,406.402713394296,406.486159229139,
406.569623824377,406.653177009799,406.736774843372,406.820506406234,406.9003402447,
406.984086977402,407.067730654418,407.151291398484,407.234789260441,407.318251761003,
407.401696896496,407.485142731338,407.568607326576,407.652160511998,407.735758345571,
407.819489908433,407.899323746899,407.983070479601,408.066714156617,408.150274900683,
408.23377276264,408.317235263202,408.400680398694,408.484126233537,408.567590828775,
408.651144014197,408.73474184777,408.818473410631,408.898307249098,408.9820539818,
409.065697658816,409.149258402883,409.23275626484,409.316218765402,409.399663900895,
409.483109735738,409.566574330976,409.650127516398,409.73372534997,409.817456912832,
409.897290751298,409.981037484,410.064681161016,410.148241905082,410.231739767039,
410.315202267601,410.398647403093,410.482093237936,410.565557833174,410.649111018596,
410.732708852169,410.816440415031,410.896274253497,410.980187398237,411.063998149748,
411.147724505201,411.23138439992,411.314997651452,411.398582238589,411.482174468518,
411.548637620264),.UNSPECIFIED.);
#352=B_SPLINE_CURVE_WITH_KNOTS('',3,(#32925,#32926,#32927,#32928,#32929,
#32930,#32931,#32932,#32933,#32934,#32935,#32936,#32937,#32938,#32939,#32940,
#32941,#32942,#32943,#32944,#32945,#32946,#32947,#32948,#32949,#32950,#32951,
#32952,#32953,#32954,#32955,#32956,#32957,#32958,#32959,#32960,#32961,#32962,
#32963,#32964,#32965,#32966,#32967,#32968,#32969,#32970,#32971,#32972,#32973,
#32974,#32975,#32976,#32977,#32978,#32979,#32980,#32981,#32982,#32983,#32984,
#32985,#32986,#32987,#32988,#32989,#32990,#32991,#32992,#32993,#32994,#32995,
#32996,#32997,#32998,#32999,#33000,#33001,#33002,#33003,#33004,#33005,#33006,
#33007,#33008,#33009,#33010,#33011,#33012,#33013,#33014,#33015,#33016,#33017,
#33018,#33019,#33020,#33021,#33022,#33023,#33024,#33025,#33026,#33027,#33028,
#33029,#33030,#33031,#33032,#33033,#33034,#33035,#33036,#33037,#33038,#33039,
#33040,#33041,#33042,#33043,#33044,#33045,#33046,#33047,#33048,#33049,#33050,
#33051,#33052,#33053,#33054,#33055,#33056,#33057,#33058,#33059,#33060,#33061,
#33062,#33063,#33064,#33065,#33066,#33067,#33068,#33069,#33070,#33071,#33072,
#33073,#33074,#33075,#33076,#33077,#33078,#33079,#33080,#33081,#33082,#33083,
#33084,#33085,#33086,#33087,#33088,#33089,#33090,#33091,#33092,#33093,#33094,
#33095,#33096,#33097,#33098,#33099,#33100,#33101,#33102,#33103,#33104,#33105,
#33106,#33107,#33108,#33109,#33110,#33111,#33112,#33113,#33114,#33115,#33116,
#33117,#33118,#33119,#33120,#33121,#33122,#33123,#33124,#33125,#33126,#33127,
#33128,#33129,#33130,#33131,#33132,#33133,#33134,#33135,#33136,#33137,#33138,
#33139,#33140,#33141,#33142,#33143,#33144,#33145,#33146,#33147,#33148,#33149,
#33150,#33151,#33152,#33153),.UNSPECIFIED.,.F.,.F.,(4,3,3,3,3,3,3,3,3,3,
3,3,3,3,3,3,3,3,3,3,3,3,3,3,3,3,3,3,3,3,3,3,3,3,3,3,3,3,3,3,3,3,3,3,3,3,
3,3,3,3,3,3,3,3,3,3,3,3,3,3,3,3,3,3,3,3,3,3,3,3,3,3,3,3,3,3,4),(398.98226700603,
399.065122617391,399.147881411393,399.230564299258,399.315175728014,399.397778478442,
399.480372809342,399.562977498193,399.649097055971,399.731823868288,399.81460673228,
399.897502480361,399.907455729306,399.991202462008,400.074846139024,400.15840688309,
400.241904745047,400.32536724561,400.408812381102,400.492258215945,400.575722811182,
400.659275996604,400.742873830177,400.826605393039,400.906439231505,400.990185964207,
401.073829641223,401.157390385289,401.240888247246,401.324350747808,401.407795883301,
401.491241718143,401.574706313381,401.658259498803,401.741857332376,401.825588895238,
401.905422733704,401.989169466406,402.072813143422,402.156373887489,402.239871749446,
402.323334250008,402.406779385501,402.490225220344,402.573689815582,402.657243001004,
402.740840834576,402.824572397438,402.904406235903,402.988152968605,403.071796645621,
403.155357389687,403.238855251644,403.322317752207,403.405762887699,403.489208722542,
403.57267331778,403.656226503202,403.739824336775,403.823555899637,403.903389738103,
403.987136470805,404.070780147821,404.154340891888,404.237838753845,404.321301254408,
404.4047463899,404.488192224743,404.571656819981,404.655210005403,404.738807838976,
404.822539401838,404.902373240302,404.998091733373,405.093477072523,405.188223685256,
405.265452312886),.UNSPECIFIED.);
#353=B_SPLINE_CURVE_WITH_KNOTS('',3,(#33155,#33156,#33157,#33158,#33159,
#33160,#33161,#33162,#33163,#33164,#33165,#33166,#33167,#33168,#33169,#33170,
#33171,#33172,#33173,#33174,#33175,#33176,#33177,#33178,#33179,#33180,#33181,
#33182,#33183,#33184,#33185,#33186,#33187,#33188,#33189,#33190,#33191,#33192,
#33193,#33194,#33195,#33196,#33197,#33198,#33199,#33200,#33201,#33202,#33203,
#33204,#33205,#33206,#33207,#33208,#33209,#33210,#33211,#33212,#33213,#33214,
#33215,#33216,#33217,#33218,#33219,#33220,#33221,#33222,#33223,#33224,#33225,
#33226,#33227,#33228,#33229,#33230,#33231,#33232,#33233,#33234,#33235,#33236,
#33237,#33238,#33239,#33240,#33241,#33242,#33243,#33244,#33245,#33246,#33247,
#33248,#33249,#33250,#33251,#33252,#33253,#33254,#33255,#33256,#33257,#33258,
#33259,#33260,#33261,#33262,#33263,#33264,#33265,#33266,#33267,#33268,#33269,
#33270,#33271,#33272,#33273,#33274,#33275,#33276,#33277,#33278,#33279,#33280,
#33281,#33282,#33283,#33284,#33285,#33286,#33287,#33288,#33289,#33290,#33291,
#33292,#33293,#33294,#33295,#33296,#33297,#33298,#33299,#33300,#33301,#33302,
#33303,#33304,#33305,#33306,#33307,#33308,#33309,#33310,#33311,#33312,#33313,
#33314,#33315,#33316,#33317,#33318,#33319,#33320,#33321,#33322,#33323,#33324,
#33325,#33326,#33327,#33328,#33329,#33330,#33331,#33332,#33333,#33334,#33335,
#33336,#33337,#33338,#33339,#33340,#33341,#33342,#33343,#33344,#33345,#33346,
#33347,#33348,#33349,#33350,#33351,#33352,#33353,#33354,#33355,#33356,#33357,
#33358,#33359,#33360,#33361,#33362,#33363,#33364,#33365,#33366,#33367,#33368,
#33369,#33370,#33371,#33372,#33373,#33374,#33375,#33376,#33377,#33378,#33379,
#33380),.UNSPECIFIED.,.F.,.F.,(4,3,3,3,3,3,3,3,3,3,3,3,3,3,3,3,3,3,3,3,
3,3,3,3,3,3,3,3,3,3,3,3,3,3,3,3,3,3,3,3,3,3,3,3,3,3,3,3,3,3,3,3,3,3,3,3,
3,3,3,3,3,3,3,3,3,3,3,3,3,3,3,3,3,3,3,4),(392.699081698725,392.814856252697,
392.914571213912,392.998317946614,393.08196162363,393.165522367697,393.249020229654,
393.332482730216,393.415927865709,393.499373700552,393.58283829579,393.666391481212,
393.749989314785,393.833720877646,393.913554716111,393.997301448813,394.080945125829,
394.164505869895,394.248003731852,394.331466232415,394.414911367907,394.49835720275,
394.581821797988,394.66537498341,394.748972816982,394.832704379844,394.91253821831,
394.996284951012,395.079928628028,395.163489372094,395.246987234051,395.330449734613,
395.413894870105,395.497340704948,395.580805300186,395.664358485608,395.74795631918,
395.831687882042,395.911521720509,395.995268453211,396.078912130227,396.162472874293,
396.24597073625,396.329433236813,396.412878372305,396.496324207148,396.579788802386,
396.663341987808,396.746939821381,396.830671384243,396.910505222708,396.99425195541,
397.077895632426,397.161456376492,397.244954238449,397.328416739012,397.411861874504,
397.495307709347,397.578772304585,397.662325490007,397.74592332358,397.829654886441,
397.909488724908,397.99323545761,398.076879134626,398.160439878693,398.243937740649,
398.327400241212,398.410845376704,398.494291211547,398.577755806786,398.661308992208,
398.74490682578,398.828638388642,398.908472227107,398.982267005905),
 .UNSPECIFIED.);
#354=B_SPLINE_CURVE_WITH_KNOTS('',3,(#33382,#33383,#33384,#33385,#33386,
#33387,#33388,#33389,#33390,#33391,#33392,#33393,#33394,#33395,#33396,#33397,
#33398,#33399,#33400,#33401,#33402,#33403,#33404,#33405,#33406,#33407,#33408,
#33409,#33410,#33411,#33412,#33413,#33414,#33415,#33416,#33417,#33418,#33419,
#33420,#33421,#33422,#33423,#33424,#33425,#33426,#33427,#33428,#33429,#33430,
#33431,#33432,#33433,#33434,#33435,#33436,#33437,#33438,#33439,#33440,#33441,
#33442,#33443,#33444,#33445,#33446,#33447,#33448,#33449,#33450,#33451,#33452,
#33453,#33454,#33455,#33456,#33457,#33458,#33459,#33460,#33461,#33462,#33463,
#33464,#33465,#33466,#33467,#33468,#33469,#33470,#33471,#33472,#33473,#33474,
#33475,#33476,#33477,#33478,#33479,#33480,#33481,#33482,#33483,#33484,#33485,
#33486,#33487,#33488,#33489,#33490,#33491,#33492,#33493,#33494,#33495,#33496,
#33497,#33498,#33499,#33500,#33501,#33502,#33503,#33504,#33505,#33506,#33507,
#33508,#33509,#33510,#33511,#33512,#33513,#33514,#33515,#33516,#33517,#33518,
#33519,#33520,#33521,#33522,#33523,#33524,#33525,#33526,#33527,#33528,#33529,
#33530,#33531,#33532,#33533,#33534,#33535,#33536,#33537,#33538,#33539,#33540,
#33541,#33542,#33543,#33544,#33545,#33546,#33547,#33548,#33549,#33550,#33551,
#33552,#33553,#33554,#33555,#33556,#33557,#33558,#33559,#33560,#33561,#33562,
#33563,#33564,#33565,#33566,#33567,#33568,#33569,#33570,#33571,#33572,#33573,
#33574,#33575,#33576,#33577,#33578,#33579,#33580,#33581,#33582,#33583,#33584,
#33585,#33586,#33587,#33588,#33589,#33590,#33591,#33592,#33593,#33594,#33595,
#33596,#33597,#33598,#33599,#33600,#33601,#33602,#33603,#33604,#33605,#33606,
#33607,#33608,#33609,#33610),.UNSPECIFIED.,.F.,.F.,(4,3,3,3,3,3,3,3,3,3,
3,3,3,3,3,3,3,3,3,3,3,3,3,3,3,3,3,3,3,3,3,3,3,3,3,3,3,3,3,3,3,3,3,3,3,3,
3,3,3,3,3,3,3,3,3,3,3,3,3,3,3,3,3,3,3,3,3,3,3,3,3,3,3,3,3,3,4),(386.415896391546,
386.50311517261,386.59044188571,386.677968044926,386.765598608585,386.853428582552,
386.920670200717,387.004416933419,387.088060610435,387.171621354501,387.255119216458,
387.338581717021,387.422026852513,387.505472687356,387.588937282594,387.672490468016,
387.756088301589,387.839819864451,387.919653702916,388.003400435618,388.087044112634,
388.1706048567,388.254102718657,388.33756521922,388.421010354712,388.504456189555,
388.587920784793,388.671473970215,388.755071803787,388.838803366649,388.918637205115,
389.002383937817,389.086027614833,389.169588358899,389.253086220856,389.336548721418,
389.419993856911,389.503439691753,389.586904286991,389.670457472413,389.754055305986,
389.837786868848,389.917620707314,390.001367440016,390.085011117032,390.168571861098,
390.252069723055,390.335532223617,390.41897735911,390.502423193952,390.585887789191,
390.669440974613,390.753038808186,390.836770371047,390.916604209513,391.000350942215,
391.083994619231,391.167555363297,391.251053225254,391.334515725817,391.417960861309,
391.501406696152,391.58487129139,391.668424476812,391.752022310385,391.835753873247,
391.915587711713,391.998183342791,392.080675349664,392.163072226687,392.24541584479,
392.327725220785,392.410019339919,392.492345036332,392.574687966156,392.65710402368,
392.699081698622),.UNSPECIFIED.);
#355=B_SPLINE_CURVE_WITH_KNOTS('',3,(#33612,#33613,#33614,#33615,#33616,
#33617,#33618,#33619,#33620,#33621,#33622,#33623,#33624,#33625,#33626,#33627,
#33628,#33629,#33630,#33631,#33632,#33633,#33634,#33635,#33636,#33637,#33638,
#33639,#33640,#33641,#33642,#33643,#33644,#33645,#33646,#33647,#33648,#33649,
#33650,#33651,#33652,#33653,#33654,#33655,#33656,#33657,#33658,#33659,#33660,
#33661,#33662,#33663,#33664,#33665,#33666,#33667,#33668,#33669,#33670,#33671,
#33672,#33673,#33674,#33675,#33676,#33677,#33678,#33679,#33680,#33681,#33682,
#33683,#33684,#33685,#33686,#33687,#33688,#33689,#33690,#33691,#33692,#33693,
#33694,#33695,#33696,#33697,#33698,#33699,#33700,#33701,#33702,#33703,#33704,
#33705,#33706,#33707,#33708,#33709,#33710,#33711,#33712,#33713,#33714,#33715,
#33716,#33717,#33718,#33719,#33720,#33721,#33722,#33723,#33724,#33725,#33726,
#33727,#33728,#33729,#33730,#33731,#33732,#33733,#33734,#33735,#33736,#33737,
#33738,#33739,#33740,#33741,#33742,#33743,#33744,#33745,#33746,#33747,#33748,
#33749,#33750,#33751,#33752,#33753,#33754,#33755,#33756,#33757,#33758,#33759,
#33760,#33761,#33762,#33763,#33764,#33765,#33766,#33767,#33768,#33769,#33770,
#33771,#33772,#33773,#33774,#33775,#33776,#33777,#33778,#33779,#33780,#33781,
#33782,#33783,#33784,#33785,#33786,#33787,#33788,#33789,#33790,#33791,#33792,
#33793,#33794,#33795,#33796,#33797,#33798,#33799,#33800,#33801,#33802,#33803,
#33804,#33805,#33806,#33807,#33808,#33809,#33810,#33811,#33812,#33813,#33814,
#33815,#33816,#33817,#33818,#33819,#33820,#33821,#33822,#33823,#33824,#33825,
#33826,#33827,#33828,#33829,#33830,#33831,#33832,#33833,#33834,#33835,#33836,
#33837,#33838,#33839,#33840),.UNSPECIFIED.,.F.,.F.,(4,3,3,3,3,3,3,3,3,3,
3,3,3,3,3,3,3,3,3,3,3,3,3,3,3,3,3,3,3,3,3,3,3,3,3,3,3,3,3,3,3,3,3,3,3,3,
3,3,3,3,3,3,3,3,3,3,3,3,3,3,3,3,3,3,3,3,3,3,3,3,3,3,3,3,3,3,4),(380.132711084533,
380.21510704019,380.297435606509,380.379723757588,380.461992342737,380.544260359157,
380.626546801328,380.708918082886,380.79133548327,380.873875988774,380.926769187522,
381.010515920224,381.09415959724,381.177720341306,381.261218203263,381.344680703826,
381.428125839318,381.511571674161,381.595036269399,381.678589454821,381.762187288394,
381.845918851256,381.925752689721,382.009499422423,382.093143099439,382.176703843505,
382.260201705462,382.343664206024,382.427109341516,382.510555176359,382.594019771597,
382.677572957019,382.761170790592,382.844902353453,382.92473619192,383.008482924622,
383.092126601638,383.175687345704,383.259185207661,383.342647708224,383.426092843716,
383.509538678559,383.593003273797,383.676556459219,383.760154292791,383.843885855653,
383.923719694119,384.007466426821,384.091110103837,384.174670847903,384.25816870986,
384.341631210422,384.425076345915,384.508522180758,384.591986775996,384.675539961417,
384.75913779499,384.842869357852,384.922703196318,385.00644992902,385.090093606036,
385.173654350103,385.25715221206,385.340614712623,385.424059848115,385.507505682958,
385.590970278196,385.674523463618,385.75812129719,385.841852860052,385.921686698518,
386.009955113066,386.098068483732,386.18597518154,386.273758263555,386.361377828746,
386.415896391433),.UNSPECIFIED.);
#356=B_SPLINE_CURVE_WITH_KNOTS('',3,(#33842,#33843,#33844,#33845,#33846,
#33847,#33848,#33849,#33850,#33851,#33852,#33853,#33854,#33855,#33856,#33857,
#33858,#33859,#33860,#33861,#33862,#33863,#33864,#33865,#33866,#33867,#33868,
#33869,#33870,#33871,#33872,#33873,#33874,#33875,#33876,#33877,#33878,#33879,
#33880,#33881,#33882,#33883,#33884,#33885,#33886,#33887,#33888,#33889,#33890,
#33891,#33892,#33893,#33894,#33895,#33896,#33897,#33898,#33899,#33900,#33901,
#33902,#33903,#33904,#33905,#33906,#33907,#33908,#33909,#33910,#33911,#33912,
#33913,#33914,#33915,#33916,#33917,#33918,#33919,#33920,#33921,#33922,#33923,
#33924,#33925,#33926,#33927,#33928,#33929,#33930,#33931,#33932,#33933,#33934,
#33935,#33936,#33937,#33938,#33939,#33940,#33941,#33942,#33943,#33944,#33945,
#33946,#33947,#33948,#33949,#33950,#33951,#33952,#33953,#33954,#33955,#33956,
#33957,#33958,#33959,#33960,#33961,#33962,#33963,#33964,#33965,#33966,#33967,
#33968,#33969,#33970,#33971,#33972,#33973,#33974,#33975,#33976,#33977,#33978,
#33979,#33980,#33981,#33982,#33983,#33984,#33985,#33986,#33987,#33988,#33989,
#33990,#33991,#33992,#33993,#33994,#33995,#33996,#33997,#33998,#33999,#34000,
#34001,#34002,#34003,#34004,#34005,#34006,#34007,#34008,#34009,#34010,#34011,
#34012,#34013,#34014,#34015,#34016,#34017,#34018,#34019,#34020,#34021,#34022,
#34023,#34024,#34025,#34026,#34027,#34028,#34029,#34030,#34031,#34032,#34033,
#34034,#34035,#34036,#34037,#34038,#34039,#34040,#34041,#34042,#34043,#34044,
#34045,#34046,#34047,#34048,#34049,#34050,#34051,#34052,#34053,#34054,#34055,
#34056,#34057,#34058,#34059,#34060,#34061,#34062,#34063,#34064,#34065,#34066,
#34067),.UNSPECIFIED.,.F.,.F.,(4,3,3,3,3,3,3,3,3,3,3,3,3,3,3,3,3,3,3,3,
3,3,3,3,3,3,3,3,3,3,3,3,3,3,3,3,3,3,3,3,3,3,3,3,3,3,3,3,3,3,3,3,3,3,3,3,
3,3,3,3,3,3,3,3,3,3,3,3,3,3,3,3,3,3,3,4),(373.849525777186,373.933884672128,
374.01763140483,374.101275081846,374.184835825912,374.268333687869,374.351796188432,
374.435241323924,374.518687158767,374.602151754005,374.685704939427,374.769302772999,
374.853034335861,374.932868174327,375.016614907029,375.100258584045,375.183819328111,
375.267317190068,375.35077969063,375.434224826122,375.517670660965,375.601135256203,
375.684688441625,375.768286275198,375.852017838059,375.931851676526,376.015598409228,
376.099242086244,376.18280283031,376.266300692267,376.34976319283,376.433208328322,
376.516654163165,376.600118758403,376.683671943824,376.767269777397,376.851001340259,
376.930835178725,377.014581911427,377.098225588443,377.181786332509,377.265284194466,
377.348746695028,377.432191830521,377.515637665364,377.599102260602,377.682655446023,
377.766253279596,377.849984842458,377.929818680924,378.013565413626,378.097209090642,
378.180769834708,378.264267696665,378.347730197228,378.43117533272,378.514621167563,
378.598085762801,378.681638948223,378.765236781796,378.848968344657,378.928802183123,
379.012548915825,379.096192592841,379.179753336907,379.263251198864,379.346713699427,
379.430158834919,379.513604669762,379.597069265,379.680622450422,379.764220283994,
379.847951846856,379.927785685323,380.046394219483,380.132711084366),
 .UNSPECIFIED.);
#357=B_SPLINE_CURVE_WITH_KNOTS('',3,(#34069,#34070,#34071,#34072,#34073,
#34074,#34075,#34076,#34077,#34078,#34079,#34080,#34081,#34082,#34083,#34084,
#34085,#34086,#34087,#34088,#34089,#34090,#34091,#34092,#34093,#34094,#34095,
#34096,#34097,#34098,#34099,#34100,#34101,#34102,#34103,#34104,#34105,#34106,
#34107,#34108,#34109,#34110,#34111,#34112,#34113,#34114,#34115,#34116,#34117,
#34118,#34119,#34120,#34121,#34122,#34123,#34124,#34125,#34126,#34127,#34128,
#34129,#34130,#34131,#34132,#34133,#34134,#34135,#34136,#34137,#34138,#34139,
#34140,#34141,#34142,#34143,#34144,#34145,#34146,#34147,#34148,#34149,#34150,
#34151,#34152,#34153,#34154,#34155,#34156,#34157,#34158,#34159,#34160,#34161,
#34162,#34163,#34164,#34165,#34166,#34167,#34168,#34169,#34170,#34171,#34172,
#34173,#34174,#34175,#34176,#34177,#34178,#34179,#34180,#34181,#34182,#34183,
#34184,#34185,#34186,#34187,#34188,#34189,#34190,#34191,#34192,#34193,#34194,
#34195,#34196,#34197,#34198,#34199,#34200,#34201,#34202,#34203,#34204,#34205,
#34206,#34207,#34208,#34209,#34210,#34211,#34212,#34213,#34214,#34215,#34216,
#34217,#34218,#34219,#34220,#34221,#34222,#34223,#34224,#34225,#34226,#34227,
#34228,#34229,#34230,#34231,#34232,#34233,#34234,#34235,#34236,#34237,#34238,
#34239,#34240,#34241,#34242,#34243,#34244,#34245,#34246,#34247,#34248,#34249,
#34250,#34251,#34252,#34253,#34254,#34255,#34256,#34257,#34258,#34259,#34260,
#34261,#34262,#34263,#34264,#34265,#34266,#34267,#34268,#34269,#34270,#34271,
#34272,#34273,#34274,#34275,#34276,#34277,#34278,#34279,#34280,#34281,#34282,
#34283,#34284,#34285,#34286,#34287,#34288,#34289,#34290,#34291,#34292,#34293,
#34294),.UNSPECIFIED.,.F.,.F.,(4,3,3,3,3,3,3,3,3,3,3,3,3,3,3,3,3,3,3,3,
3,3,3,3,3,3,3,3,3,3,3,3,3,3,3,3,3,3,3,3,3,3,3,3,3,3,3,3,3,3,3,3,3,3,3,3,
3,3,3,3,3,3,3,3,3,3,3,3,3,3,3,3,3,3,3,4),(367.566340470201,367.660350300293,
367.754723512711,367.849614788934,367.939983658933,368.023730391635,368.107374068651,
368.190934812717,368.274432674674,368.357895175236,368.441340310729,368.524786145571,
368.608250740809,368.691803926231,368.775401759804,368.859133322666,368.938967161132,
369.022713893834,369.10635757085,369.189918314916,369.273416176873,369.356878677436,
369.440323812928,369.523769647771,369.607234243009,369.690787428431,369.774385262003,
369.858116824865,369.937950663331,370.021697396033,370.105341073049,370.188901817115,
370.272399679072,370.355862179635,370.439307315127,370.52275314997,370.606217745208,
370.68977093063,370.773368764202,370.857100327064,370.93693416553,371.020680898232,
371.104324575248,371.187885319314,371.271383181271,371.354845681833,371.438290817326,
371.521736652168,371.605201247407,371.688754432828,371.772352266401,371.856083829263,
371.935917667729,372.019664400431,372.103308077447,372.186868821513,372.27036668347,
372.353829184033,372.437274319525,372.520720154368,372.604184749606,372.687737935028,
372.7713357686,372.855067331462,372.934901169928,373.017703443352,373.100403398518,
373.183022036849,373.266335004375,373.348860249607,373.431371904164,373.513888802314,
373.597798045999,373.680421651097,373.764973714076,373.849525777054),
 .UNSPECIFIED.);
#358=B_SPLINE_CURVE_WITH_KNOTS('',3,(#34296,#34297,#34298,#34299,#34300,
#34301,#34302,#34303,#34304,#34305,#34306,#34307,#34308,#34309,#34310,#34311,
#34312,#34313,#34314,#34315,#34316,#34317,#34318,#34319,#34320,#34321,#34322,
#34323,#34324,#34325,#34326,#34327,#34328,#34329,#34330,#34331,#34332,#34333,
#34334,#34335,#34336,#34337,#34338,#34339,#34340,#34341,#34342,#34343,#34344,
#34345,#34346,#34347,#34348,#34349,#34350,#34351,#34352,#34353,#34354,#34355,
#34356,#34357,#34358,#34359,#34360,#34361,#34362,#34363,#34364,#34365,#34366,
#34367,#34368,#34369,#34370,#34371,#34372,#34373,#34374,#34375,#34376,#34377,
#34378,#34379,#34380,#34381,#34382,#34383,#34384,#34385,#34386,#34387,#34388,
#34389,#34390,#34391,#34392,#34393,#34394,#34395,#34396,#34397,#34398,#34399,
#34400,#34401,#34402,#34403,#34404,#34405,#34406,#34407,#34408,#34409,#34410,
#34411,#34412,#34413,#34414,#34415,#34416,#34417,#34418,#34419,#34420,#34421,
#34422,#34423,#34424,#34425,#34426,#34427,#34428,#34429,#34430,#34431,#34432,
#34433,#34434,#34435,#34436,#34437,#34438,#34439,#34440,#34441,#34442,#34443,
#34444,#34445,#34446,#34447,#34448,#34449,#34450,#34451,#34452,#34453,#34454,
#34455,#34456,#34457,#34458,#34459,#34460,#34461,#34462,#34463,#34464,#34465,
#34466,#34467,#34468,#34469,#34470,#34471,#34472,#34473,#34474,#34475,#34476,
#34477,#34478,#34479,#34480,#34481,#34482,#34483,#34484,#34485,#34486,#34487,
#34488,#34489,#34490,#34491,#34492,#34493,#34494,#34495,#34496,#34497,#34498,
#34499,#34500,#34501,#34502,#34503,#34504,#34505,#34506,#34507,#34508,#34509,
#34510,#34511,#34512,#34513,#34514,#34515,#34516,#34517,#34518,#34519,#34520,
#34521,#34522,#34523,#34524),.UNSPECIFIED.,.F.,.F.,(4,3,3,3,3,3,3,3,3,3,
3,3,3,3,3,3,3,3,3,3,3,3,3,3,3,3,3,3,3,3,3,3,3,3,3,3,3,3,3,3,3,3,3,3,3,3,
3,3,3,3,3,3,3,3,3,3,3,3,3,3,3,3,3,3,3,3,3,3,3,3,3,3,3,3,3,3,4),(361.283155162827,
361.366593317698,361.450019445351,361.53345154986,361.616907635409,361.700459950804,
361.784061320472,361.867802569209,361.946082645738,362.02982937844,362.113473055456,
362.197033799522,362.280531661479,362.363994162042,362.447439297534,362.530885132377,
362.614349727615,362.697902913037,362.78150074661,362.865232309471,362.945066147937,
363.028812880639,363.112456557655,363.196017301721,363.279515163678,363.36297766424,
363.446422799733,363.529868634576,363.613333229814,363.696886415236,363.780484248808,
363.86421581167,363.944049650136,364.027796382838,364.111440059854,364.19500080392,
364.278498665877,364.361961166439,364.445406301931,364.528852136774,364.612316732012,
364.695869917434,364.779467751007,364.863199313869,364.943033152335,365.026779885037,
365.110423562053,365.193984306119,365.277482168076,365.360944668638,365.44438980413,
365.527835638973,365.611300234211,365.694853419633,365.778451253206,365.862182816068,
365.942016654534,366.025763387236,366.109407064252,366.192967808319,366.276465670276,
366.359928170838,366.443373306331,366.526819141173,366.610283736411,366.693836921833,
366.777434755406,366.861166318268,366.941000156733,367.025414114052,367.109721200961,
367.193938818128,367.27808430145,367.362170923251,367.446223229521,367.530265659005,
367.566340470007),.UNSPECIFIED.);
#359=B_SPLINE_CURVE_WITH_KNOTS('',3,(#34526,#34527,#34528,#34529,#34530,
#34531,#34532,#34533,#34534,#34535,#34536,#34537,#34538,#34539,#34540,#34541,
#34542,#34543,#34544,#34545,#34546,#34547,#34548,#34549,#34550,#34551,#34552,
#34553,#34554,#34555,#34556,#34557,#34558,#34559,#34560,#34561,#34562,#34563,
#34564,#34565,#34566,#34567,#34568,#34569,#34570,#34571,#34572,#34573,#34574,
#34575,#34576,#34577,#34578,#34579,#34580,#34581,#34582,#34583,#34584,#34585,
#34586,#34587,#34588,#34589,#34590,#34591,#34592,#34593,#34594,#34595,#34596,
#34597,#34598,#34599,#34600,#34601,#34602,#34603,#34604,#34605,#34606,#34607,
#34608,#34609,#34610,#34611,#34612,#34613,#34614,#34615,#34616,#34617,#34618,
#34619,#34620,#34621,#34622,#34623,#34624,#34625,#34626,#34627,#34628,#34629,
#34630,#34631,#34632,#34633,#34634,#34635,#34636,#34637,#34638,#34639,#34640,
#34641,#34642,#34643,#34644,#34645,#34646,#34647,#34648,#34649,#34650,#34651,
#34652,#34653,#34654,#34655,#34656,#34657,#34658,#34659,#34660,#34661,#34662,
#34663,#34664,#34665,#34666,#34667,#34668,#34669,#34670,#34671,#34672,#34673,
#34674,#34675,#34676,#34677,#34678,#34679,#34680,#34681,#34682,#34683,#34684,
#34685,#34686,#34687,#34688,#34689,#34690,#34691,#34692,#34693,#34694,#34695,
#34696,#34697,#34698,#34699,#34700,#34701,#34702,#34703,#34704,#34705,#34706,
#34707,#34708,#34709,#34710,#34711,#34712,#34713,#34714,#34715,#34716,#34717,
#34718,#34719,#34720,#34721,#34722,#34723,#34724,#34725,#34726,#34727,#34728,
#34729,#34730,#34731,#34732,#34733,#34734,#34735,#34736,#34737,#34738,#34739,
#34740,#34741,#34742,#34743,#34744,#34745,#34746,#34747,#34748,#34749,#34750,
#34751,#34752,#34753,#34754),.UNSPECIFIED.,.F.,.F.,(4,3,3,3,3,3,3,3,3,3,
3,3,3,3,3,3,3,3,3,3,3,3,3,3,3,3,3,3,3,3,3,3,3,3,3,3,3,3,3,3,3,3,3,3,3,3,
3,3,3,3,3,3,3,3,3,3,3,3,3,3,3,3,3,3,3,3,3,3,3,3,3,3,3,3,3,3,4),(354.999969855836,
355.083098070547,355.166126031582,355.249074448297,355.331963953429,355.414823775889,
355.497670893546,355.580523896995,355.663401377681,355.746368482,355.82938637503,
355.912525509817,355.952181632543,356.035928365245,356.119572042261,356.203132786327,
356.286630648284,356.370093148846,356.453538284339,356.536984119182,356.62044871442,
356.704001899842,356.787599733414,356.871331296276,356.951165134742,357.034911867444,
357.11855554446,357.202116288526,357.285614150483,357.369076651045,357.452521786538,
357.53596762138,357.619432216619,357.70298540204,357.786583235613,357.870314798475,
357.950148636941,358.033895369643,358.117539046659,358.201099790725,358.284597652682,
358.368060153244,358.451505288737,358.53495112358,358.618415718817,358.701968904239,
358.785566737812,358.869298300674,358.94913213914,359.032878871842,359.116522548858,
359.200083292924,359.283581154881,359.367043655443,359.450488790935,359.533934625778,
359.617399221016,359.700952406438,359.78455024001,359.868281802872,359.948115641339,
360.031862374041,360.115506051057,360.199066795123,360.282564657079,360.366027157642,
360.449472293134,360.532918127977,360.616382723216,360.699935908638,360.78353374221,
360.867265305072,360.947099143538,361.045204785511,361.142870607703,361.239719950613,
361.283155162638),.UNSPECIFIED.);
#360=B_SPLINE_CURVE_WITH_KNOTS('',3,(#34756,#34757,#34758,#34759,#34760,
#34761,#34762,#34763,#34764,#34765,#34766,#34767,#34768,#34769,#34770,#34771,
#34772,#34773,#34774,#34775,#34776,#34777,#34778,#34779,#34780,#34781,#34782,
#34783,#34784,#34785,#34786,#34787,#34788,#34789,#34790,#34791,#34792,#34793,
#34794,#34795,#34796,#34797,#34798,#34799,#34800,#34801,#34802,#34803,#34804,
#34805,#34806,#34807,#34808,#34809,#34810,#34811,#34812,#34813,#34814,#34815,
#34816,#34817,#34818,#34819,#34820,#34821,#34822,#34823,#34824,#34825,#34826,
#34827,#34828,#34829,#34830,#34831,#34832,#34833,#34834,#34835,#34836,#34837,
#34838,#34839,#34840,#34841,#34842,#34843,#34844,#34845,#34846,#34847,#34848,
#34849,#34850,#34851,#34852,#34853,#34854,#34855,#34856,#34857,#34858,#34859,
#34860,#34861,#34862,#34863,#34864,#34865,#34866,#34867,#34868,#34869,#34870,
#34871,#34872,#34873,#34874,#34875,#34876,#34877,#34878,#34879,#34880,#34881,
#34882,#34883,#34884,#34885,#34886,#34887,#34888,#34889,#34890,#34891,#34892,
#34893,#34894,#34895,#34896,#34897,#34898,#34899,#34900,#34901,#34902,#34903,
#34904,#34905,#34906,#34907,#34908,#34909,#34910,#34911,#34912,#34913,#34914,
#34915,#34916,#34917,#34918,#34919,#34920,#34921,#34922,#34923,#34924,#34925,
#34926,#34927,#34928,#34929,#34930,#34931,#34932,#34933,#34934,#34935,#34936,
#34937,#34938,#34939,#34940,#34941,#34942,#34943,#34944,#34945,#34946,#34947,
#34948,#34949,#34950,#34951,#34952,#34953,#34954,#34955,#34956,#34957,#34958,
#34959,#34960,#34961,#34962,#34963,#34964,#34965,#34966,#34967,#34968,#34969,
#34970,#34971,#34972,#34973,#34974,#34975,#34976,#34977,#34978,#34979,#34980,
#34981,#34982,#34983,#34984),.UNSPECIFIED.,.F.,.F.,(4,3,3,3,3,3,3,3,3,3,
3,3,3,3,3,3,3,3,3,3,3,3,3,3,3,3,3,3,3,3,3,3,3,3,3,3,3,3,3,3,3,3,3,3,3,3,
3,3,3,3,3,3,3,3,3,3,3,3,3,3,3,3,3,3,3,3,3,3,3,3,3,3,3,3,3,3,4),(348.71678454857,
348.825202608615,348.936282965072,348.959297117148,349.04304384985,349.126687526866,
349.210248270933,349.293746132889,349.377208633452,349.460653768944,349.544099603787,
349.627564199025,349.711117384447,349.79471521802,349.878446780882,349.958280619348,
350.04202735205,350.125671029066,350.209231773133,350.292729635089,350.376192135652,
350.459637271144,350.543083105987,350.626547701225,350.710100886647,350.79369872022,
350.877430283082,350.957264121547,351.041010854249,351.124654531265,351.208215275331,
351.291713137288,351.37517563785,351.458620773342,351.542066608185,351.625531203423,
351.709084388845,351.792682222418,351.876413785279,351.956247623746,352.039994356448,
352.123638033464,352.20719877753,352.290696639487,352.37415914005,352.457604275542,
352.541050110385,352.624514705623,352.708067891045,352.791665724618,352.87539728748,
352.955231125945,353.038977858647,353.122621535663,353.206182279729,353.289680141686,
353.373142642248,353.456587777741,353.540033612583,353.623498207821,353.707051393243,
353.790649226816,353.874380789678,353.954214628144,354.037961360846,354.121605037862,
354.205165781928,354.288663643885,354.372126144447,354.455571279939,354.539017114782,
354.62248171002,354.706034895442,354.789632729015,354.873364291876,354.953198130343,
354.999969855648),.UNSPECIFIED.);
#361=B_SPLINE_CURVE_WITH_KNOTS('',3,(#34986,#34987,#34988,#34989,#34990,
#34991,#34992,#34993,#34994,#34995,#34996,#34997,#34998,#34999,#35000,#35001,
#35002,#35003,#35004,#35005,#35006,#35007,#35008,#35009,#35010,#35011,#35012,
#35013,#35014,#35015,#35016,#35017,#35018,#35019,#35020,#35021,#35022,#35023,
#35024,#35025,#35026,#35027,#35028,#35029,#35030,#35031,#35032,#35033,#35034,
#35035,#35036,#35037,#35038,#35039,#35040,#35041,#35042,#35043,#35044,#35045,
#35046,#35047,#35048,#35049,#35050,#35051,#35052,#35053,#35054,#35055,#35056,
#35057,#35058,#35059,#35060,#35061,#35062,#35063,#35064,#35065,#35066,#35067,
#35068,#35069,#35070,#35071,#35072,#35073,#35074,#35075,#35076,#35077,#35078,
#35079,#35080,#35081,#35082,#35083,#35084,#35085,#35086,#35087,#35088,#35089,
#35090,#35091,#35092,#35093,#35094,#35095,#35096,#35097,#35098,#35099,#35100,
#35101,#35102,#35103,#35104,#35105,#35106,#35107,#35108,#35109,#35110,#35111,
#35112,#35113,#35114,#35115,#35116,#35117,#35118,#35119,#35120,#35121,#35122,
#35123,#35124,#35125,#35126,#35127,#35128,#35129,#35130,#35131,#35132,#35133,
#35134,#35135,#35136,#35137,#35138,#35139,#35140,#35141,#35142,#35143,#35144,
#35145,#35146,#35147,#35148,#35149,#35150,#35151,#35152,#35153,#35154,#35155,
#35156,#35157,#35158,#35159,#35160,#35161,#35162,#35163,#35164,#35165,#35166,
#35167,#35168,#35169,#35170,#35171,#35172,#35173,#35174,#35175,#35176,#35177,
#35178,#35179,#35180,#35181,#35182,#35183,#35184,#35185,#35186,#35187,#35188,
#35189,#35190,#35191,#35192,#35193,#35194,#35195,#35196,#35197,#35198,#35199,
#35200,#35201,#35202,#35203,#35204,#35205,#35206,#35207,#35208,#35209,#35210,
#35211,#35212,#35213,#35214,#35215,#35216,#35217),.UNSPECIFIED.,.F.,.F.,
(4,3,3,3,3,3,3,3,3,3,3,3,3,3,3,3,3,3,3,3,3,3,3,3,3,3,3,3,3,3,3,3,3,3,3,
3,3,3,3,3,3,3,3,3,3,3,3,3,3,3,3,3,3,3,3,3,3,3,3,3,3,3,3,3,3,3,3,3,3,3,3,
3,3,3,3,3,3,4),(342.433599241289,342.51992594412,342.606329662537,342.696096272891,
342.782755320326,342.86950763198,342.956417766365,342.965396103953,343.049142836655,
343.132786513671,343.216347257738,343.299845119694,343.383307620257,343.466752755749,
343.550198590592,343.63366318583,343.717216371252,343.800814204825,343.884545767687,
343.964379606153,344.048126338855,344.131770015871,344.215330759937,344.298828621894,
344.382291122457,344.465736257949,344.549182092792,344.63264668803,344.716199873452,
344.799797707024,344.883529269886,344.963363108352,345.047109841054,345.13075351807,
345.214314262137,345.297812124093,345.381274624656,345.464719760148,345.548165594991,
345.631630190229,345.715183375651,345.798781209223,345.882512772085,345.962346610551,
346.046093343253,346.129737020269,346.213297764335,346.296795626292,346.380258126854,
346.463703262347,346.547149097189,346.630613692427,346.714166877849,346.797764711422,
346.881496274284,346.96133011275,347.045076845452,347.128720522468,347.212281266534,
347.29577912849,347.379241629053,347.462686764545,347.546132599388,347.629597194627,
347.713150380049,347.796748213621,347.880479776483,347.960313614949,348.043054505276,
348.127270760675,348.209808258655,348.292291441905,348.374739235986,348.460250564106,
348.542706853071,348.625180065633,348.707712121519,348.716784548468),
 .UNSPECIFIED.);
#362=B_SPLINE_CURVE_WITH_KNOTS('',3,(#35219,#35220,#35221,#35222,#35223,
#35224,#35225,#35226,#35227,#35228,#35229,#35230,#35231,#35232,#35233,#35234,
#35235,#35236,#35237,#35238,#35239,#35240,#35241,#35242,#35243,#35244,#35245,
#35246,#35247,#35248,#35249,#35250,#35251,#35252,#35253,#35254,#35255,#35256,
#35257,#35258,#35259,#35260,#35261,#35262,#35263,#35264,#35265,#35266,#35267,
#35268,#35269,#35270,#35271,#35272,#35273,#35274,#35275,#35276,#35277,#35278,
#35279,#35280,#35281,#35282,#35283,#35284,#35285,#35286,#35287,#35288,#35289,
#35290,#35291,#35292,#35293,#35294,#35295,#35296,#35297,#35298,#35299,#35300,
#35301,#35302,#35303,#35304,#35305,#35306,#35307,#35308,#35309,#35310,#35311,
#35312,#35313,#35314,#35315,#35316,#35317,#35318,#35319,#35320,#35321,#35322,
#35323,#35324,#35325,#35326,#35327,#35328,#35329,#35330,#35331,#35332,#35333,
#35334,#35335,#35336,#35337,#35338,#35339,#35340,#35341,#35342,#35343,#35344,
#35345,#35346,#35347,#35348,#35349,#35350,#35351,#35352,#35353,#35354,#35355,
#35356,#35357,#35358,#35359,#35360,#35361,#35362,#35363,#35364,#35365,#35366,
#35367,#35368,#35369,#35370,#35371,#35372,#35373,#35374,#35375,#35376,#35377,
#35378,#35379,#35380,#35381,#35382,#35383,#35384,#35385,#35386,#35387,#35388,
#35389,#35390,#35391,#35392,#35393,#35394,#35395,#35396,#35397,#35398,#35399,
#35400,#35401,#35402,#35403,#35404,#35405,#35406,#35407,#35408,#35409,#35410,
#35411,#35412,#35413,#35414,#35415,#35416,#35417,#35418,#35419,#35420,#35421,
#35422,#35423,#35424,#35425,#35426,#35427,#35428,#35429,#35430,#35431,#35432,
#35433,#35434,#35435,#35436,#35437,#35438,#35439,#35440,#35441,#35442,#35443,
#35444,#35445,#35446,#35447),.UNSPECIFIED.,.F.,.F.,(4,3,3,3,3,3,3,3,3,3,
3,3,3,3,3,3,3,3,3,3,3,3,3,3,3,3,3,3,3,3,3,3,3,3,3,3,3,3,3,3,3,3,3,3,3,3,
3,3,3,3,3,3,3,3,3,3,3,3,3,3,3,3,3,3,3,3,3,3,3,3,3,3,3,3,3,3,4),(336.150413934269,
336.232787324844,336.315085749949,336.397333675145,336.479555269055,336.561769565653,
336.643995590724,336.726302690793,336.8086499515,336.891127738289,336.971495090759,
337.055241823461,337.138885500477,337.222446244543,337.3059441065,337.389406607062,
337.472851742555,337.556297577398,337.639762172636,337.723315358057,337.80691319163,
337.890644754492,337.970478592958,338.05422532566,338.137869002676,338.221429746743,
338.304927608699,338.388390109262,338.471835244754,338.555281079597,338.638745674835,
338.722298860257,338.80589669383,338.889628256692,338.969462095157,339.053208827859,
339.136852504875,339.220413248941,339.303911110898,339.38737361146,339.470818746952,
339.554264581795,339.637729177033,339.721282362455,339.804880196028,339.888611758889,
339.968445597356,340.052192330058,340.135836007074,340.21939675114,340.302894613097,
340.386357113659,340.469802249152,340.553248083995,340.636712679232,340.720265864654,
340.803863698227,340.887595261089,340.967429099555,341.051175832257,341.134819509273,
341.21838025334,341.301878115297,341.385340615859,341.468785751352,341.552231586195,
341.635696181433,341.719249366855,341.802847200427,341.886578763289,341.966412601754,
342.055853088888,342.145118135785,342.234139928017,342.323010439427,342.411678679605,
342.433599241143),.UNSPECIFIED.);
#363=B_SPLINE_CURVE_WITH_KNOTS('',3,(#35449,#35450,#35451,#35452,#35453,
#35454,#35455,#35456,#35457,#35458,#35459,#35460,#35461,#35462,#35463,#35464,
#35465,#35466,#35467,#35468,#35469,#35470,#35471,#35472,#35473,#35474,#35475,
#35476,#35477,#35478,#35479,#35480,#35481,#35482,#35483,#35484,#35485,#35486,
#35487,#35488,#35489,#35490,#35491,#35492,#35493,#35494,#35495,#35496,#35497,
#35498,#35499,#35500,#35501,#35502,#35503,#35504,#35505,#35506,#35507,#35508,
#35509,#35510,#35511,#35512,#35513,#35514,#35515,#35516,#35517,#35518,#35519,
#35520,#35521,#35522,#35523,#35524,#35525,#35526,#35527,#35528,#35529,#35530,
#35531,#35532,#35533,#35534,#35535,#35536,#35537,#35538,#35539,#35540,#35541,
#35542,#35543,#35544,#35545,#35546,#35547,#35548,#35549,#35550,#35551,#35552,
#35553,#35554,#35555,#35556,#35557,#35558,#35559,#35560,#35561,#35562,#35563,
#35564,#35565,#35566,#35567,#35568,#35569,#35570,#35571,#35572,#35573,#35574,
#35575,#35576,#35577,#35578,#35579,#35580,#35581,#35582,#35583,#35584,#35585,
#35586,#35587,#35588,#35589,#35590,#35591,#35592,#35593,#35594,#35595,#35596,
#35597,#35598,#35599,#35600,#35601,#35602,#35603,#35604,#35605,#35606,#35607,
#35608,#35609,#35610,#35611,#35612,#35613,#35614,#35615,#35616,#35617,#35618,
#35619,#35620,#35621,#35622,#35623,#35624,#35625,#35626,#35627,#35628,#35629,
#35630,#35631,#35632,#35633,#35634,#35635,#35636,#35637,#35638,#35639,#35640,
#35641,#35642,#35643,#35644,#35645,#35646,#35647,#35648,#35649,#35650,#35651,
#35652,#35653,#35654,#35655,#35656,#35657,#35658,#35659,#35660,#35661,#35662,
#35663,#35664,#35665,#35666,#35667,#35668,#35669,#35670,#35671,#35672,#35673,
#35674),.UNSPECIFIED.,.F.,.F.,(4,3,3,3,3,3,3,3,3,3,3,3,3,3,3,3,3,3,3,3,
3,3,3,3,3,3,3,3,3,3,3,3,3,3,3,3,3,3,3,3,3,3,3,3,3,3,3,3,3,3,3,3,3,3,3,3,
3,3,3,3,3,3,3,3,3,3,3,3,3,3,3,3,3,3,3,4),(329.867228626929,329.978610575364,
330.062357308066,330.146000985082,330.229561729148,330.313059591105,330.396522091667,
330.479967227159,330.563413062002,330.64687765724,330.730430842662,330.814028676234,
330.897760239096,330.977594077564,331.061340810266,331.144984487282,331.228545231348,
331.312043093305,331.395505593868,331.47895072936,331.562396564203,331.645861159441,
331.729414344863,331.813012178436,331.896743741298,331.976577579763,332.060324312465,
332.143967989481,332.227528733547,332.311026595504,332.394489096066,332.477934231559,
332.561380066401,332.64484466164,332.728397847061,332.811995680634,332.895727243496,
332.975561081962,333.059307814664,333.14295149168,333.226512235746,333.310010097703,
333.393472598265,333.476917733758,333.560363568601,333.643828163839,333.72738134926,
333.810979182833,333.894710745695,333.974544584161,334.058291316863,334.141934993879,
334.225495737945,334.308993599902,334.392456100465,334.475901235957,334.5593470708,
334.642811666038,334.72636485146,334.809962685032,334.893694247894,334.97352808636,
335.057274819062,335.140918496078,335.224479240144,335.307977102101,335.391439602663,
335.474884738155,335.558330572998,335.641795168236,335.725348353658,335.80894618723,
335.892677750092,335.972511588559,336.100376929765,336.150413934109),
 .UNSPECIFIED.);
#364=B_SPLINE_CURVE_WITH_KNOTS('',3,(#35676,#35677,#35678,#35679,#35680,
#35681,#35682,#35683,#35684,#35685,#35686,#35687,#35688,#35689,#35690,#35691,
#35692,#35693,#35694,#35695,#35696,#35697,#35698,#35699,#35700,#35701,#35702,
#35703,#35704,#35705,#35706,#35707,#35708,#35709,#35710,#35711,#35712,#35713,
#35714,#35715,#35716,#35717,#35718,#35719,#35720,#35721,#35722,#35723,#35724,
#35725,#35726,#35727,#35728,#35729,#35730,#35731,#35732,#35733,#35734,#35735,
#35736,#35737,#35738,#35739,#35740,#35741,#35742,#35743,#35744,#35745,#35746,
#35747,#35748,#35749,#35750,#35751,#35752,#35753,#35754,#35755,#35756,#35757,
#35758,#35759,#35760,#35761,#35762,#35763,#35764,#35765,#35766,#35767,#35768,
#35769,#35770,#35771,#35772,#35773,#35774,#35775,#35776,#35777,#35778,#35779,
#35780,#35781,#35782,#35783,#35784,#35785,#35786,#35787,#35788,#35789,#35790,
#35791,#35792,#35793,#35794,#35795,#35796,#35797,#35798,#35799,#35800,#35801,
#35802,#35803,#35804,#35805,#35806,#35807,#35808,#35809,#35810,#35811,#35812,
#35813,#35814,#35815,#35816,#35817,#35818,#35819,#35820,#35821,#35822,#35823,
#35824,#35825,#35826,#35827,#35828,#35829,#35830,#35831,#35832,#35833,#35834,
#35835,#35836,#35837,#35838,#35839,#35840,#35841,#35842,#35843,#35844,#35845,
#35846,#35847,#35848,#35849,#35850,#35851,#35852,#35853,#35854,#35855,#35856,
#35857,#35858,#35859,#35860,#35861,#35862,#35863,#35864,#35865,#35866,#35867,
#35868,#35869,#35870,#35871,#35872,#35873,#35874,#35875,#35876,#35877,#35878,
#35879,#35880,#35881,#35882,#35883,#35884,#35885,#35886,#35887,#35888,#35889,
#35890,#35891,#35892,#35893,#35894,#35895,#35896,#35897,#35898,#35899,#35900,
#35901,#35902,#35903,#35904),.UNSPECIFIED.,.F.,.F.,(4,3,3,3,3,3,3,3,3,3,
3,3,3,3,3,3,3,3,3,3,3,3,3,3,3,3,3,3,3,3,3,3,3,3,3,3,3,3,3,3,3,3,3,3,3,3,
3,3,3,3,3,3,3,3,3,3,3,3,3,3,3,3,3,3,3,3,3,3,3,3,3,3,3,3,3,3,4),(323.584043319926,
323.676068069459,323.768582031357,323.861348955712,323.954448704799,323.984709562169,
324.068456294871,324.152099971887,324.235660715953,324.31915857791,324.402621078473,
324.486066213965,324.569512048808,324.652976644046,324.736529829468,324.82012766304,
324.903859225902,324.983693064369,325.067439797071,325.151083474087,325.234644218154,
325.31814208011,325.401604580673,325.485049716165,325.568495551008,325.651960146246,
325.735513331668,325.819111165241,325.902842728103,325.982676566568,326.06642329927,
326.150066976286,326.233627720352,326.317125582309,326.400588082871,326.484033218363,
326.567479053206,326.650943648444,326.734496833866,326.818094667439,326.9018262303,
326.981660068767,327.065406801469,327.149050478485,327.232611222551,327.316109084508,
327.399571585071,327.483016720563,327.566462555406,327.649927150644,327.733480336066,
327.817078169638,327.9008097325,327.980643570966,328.064390303668,328.148033980684,
328.23159472475,328.315092586707,328.398555087269,328.482000222762,328.565446057604,
328.648910652842,328.732463838264,328.816061671837,328.899793234699,328.979627073165,
329.06226410214,329.144798916669,329.227252644958,329.309645552602,329.392006139001,
329.474353359022,329.556706154076,329.639126207836,329.72158115159,329.804147275148,
329.867228626794),.UNSPECIFIED.);
#365=B_SPLINE_CURVE_WITH_KNOTS('',3,(#35906,#35907,#35908,#35909,#35910,
#35911,#35912,#35913,#35914,#35915,#35916,#35917,#35918,#35919,#35920,#35921,
#35922,#35923,#35924,#35925,#35926,#35927,#35928,#35929,#35930,#35931,#35932,
#35933,#35934,#35935,#35936,#35937,#35938,#35939,#35940,#35941,#35942,#35943,
#35944,#35945,#35946,#35947,#35948,#35949,#35950,#35951,#35952,#35953,#35954,
#35955,#35956,#35957,#35958,#35959,#35960,#35961,#35962,#35963,#35964,#35965,
#35966,#35967,#35968,#35969,#35970,#35971,#35972,#35973,#35974,#35975,#35976,
#35977,#35978,#35979,#35980,#35981,#35982,#35983,#35984,#35985,#35986,#35987,
#35988,#35989,#35990,#35991,#35992,#35993,#35994,#35995,#35996,#35997,#35998,
#35999,#36000,#36001,#36002,#36003,#36004,#36005,#36006,#36007,#36008,#36009,
#36010,#36011,#36012,#36013,#36014,#36015,#36016,#36017,#36018,#36019,#36020,
#36021,#36022,#36023,#36024,#36025,#36026,#36027,#36028,#36029,#36030,#36031,
#36032,#36033,#36034,#36035,#36036,#36037,#36038,#36039,#36040,#36041,#36042,
#36043,#36044,#36045,#36046,#36047,#36048,#36049,#36050,#36051,#36052,#36053,
#36054,#36055,#36056,#36057,#36058,#36059,#36060,#36061,#36062,#36063,#36064,
#36065,#36066,#36067,#36068,#36069,#36070,#36071,#36072,#36073,#36074,#36075,
#36076,#36077,#36078,#36079,#36080,#36081,#36082,#36083,#36084,#36085,#36086,
#36087,#36088,#36089,#36090,#36091,#36092,#36093,#36094,#36095,#36096,#36097,
#36098,#36099,#36100,#36101,#36102,#36103,#36104,#36105,#36106,#36107,#36108,
#36109,#36110,#36111,#36112,#36113,#36114,#36115,#36116,#36117,#36118,#36119,
#36120,#36121,#36122,#36123,#36124,#36125,#36126,#36127,#36128,#36129,#36130,
#36131,#36132,#36133,#36134),.UNSPECIFIED.,.F.,.F.,(4,3,3,3,3,3,3,3,3,3,
3,3,3,3,3,3,3,3,3,3,3,3,3,3,3,3,3,3,3,3,3,3,3,3,3,3,3,3,3,3,3,3,3,3,3,3,
3,3,3,3,3,3,3,3,3,3,3,3,3,3,3,3,3,3,3,3,3,3,3,3,3,3,3,3,3,3,4),(317.30085801257,
317.387101829621,317.470165711623,317.553225128186,317.636298457177,317.719404082366,
317.802606138314,317.885865515104,317.96924500468,317.990808548974,318.074555281676,
318.158198958692,318.241759702758,318.325257564715,318.408720065278,318.49216520077,
318.575611035613,318.659075630852,318.742628816274,318.826226649846,318.909958212708,
318.989792051174,319.073538783876,319.157182460892,319.240743204958,319.324241066915,
319.407703567478,319.49114870297,319.574594537813,319.658059133051,319.741612318473,
319.825210152046,319.908941714908,319.988775553373,320.072522286075,320.156165963091,
320.239726707157,320.323224569114,320.406687069677,320.490132205169,320.573578040012,
320.65704263525,320.740595820671,320.824193654244,320.907925217106,320.987759055572,
321.071505788274,321.15514946529,321.238710209356,321.322208071313,321.405670571875,
321.489115707368,321.57256154221,321.656026137448,321.73957932287,321.823177156443,
321.906908719305,321.986742557771,322.070489290473,322.154132967489,322.237693711555,
322.321191573512,322.404654074075,322.488099209567,322.57154504441,322.655009639648,
322.73856282507,322.822160658643,322.905892221504,322.98572605997,323.070728963304,
323.15561926755,323.240413521352,323.326320970951,323.410962115911,323.497502717831,
323.58404331975),.UNSPECIFIED.);
#366=B_SPLINE_CURVE_WITH_KNOTS('',3,(#36136,#36137,#36138,#36139,#36140,
#36141,#36142,#36143,#36144,#36145,#36146,#36147,#36148,#36149,#36150,#36151,
#36152,#36153,#36154,#36155,#36156,#36157,#36158,#36159,#36160,#36161,#36162,
#36163,#36164,#36165,#36166,#36167,#36168,#36169,#36170,#36171,#36172,#36173,
#36174,#36175,#36176,#36177,#36178,#36179,#36180,#36181,#36182,#36183,#36184,
#36185,#36186,#36187,#36188,#36189,#36190,#36191,#36192,#36193,#36194,#36195,
#36196,#36197,#36198,#36199,#36200,#36201,#36202,#36203,#36204,#36205,#36206,
#36207,#36208,#36209,#36210,#36211,#36212,#36213,#36214,#36215,#36216,#36217,
#36218,#36219,#36220,#36221,#36222,#36223,#36224,#36225,#36226,#36227,#36228,
#36229,#36230,#36231,#36232,#36233,#36234,#36235,#36236,#36237,#36238,#36239,
#36240,#36241,#36242,#36243,#36244,#36245,#36246,#36247,#36248,#36249,#36250,
#36251,#36252,#36253,#36254,#36255,#36256,#36257,#36258,#36259,#36260,#36261,
#36262,#36263,#36264,#36265,#36266,#36267,#36268,#36269,#36270,#36271,#36272,
#36273,#36274,#36275,#36276,#36277,#36278,#36279,#36280,#36281,#36282,#36283,
#36284,#36285,#36286,#36287,#36288,#36289,#36290,#36291,#36292,#36293,#36294,
#36295,#36296,#36297,#36298,#36299,#36300,#36301,#36302,#36303,#36304,#36305,
#36306,#36307,#36308,#36309,#36310,#36311,#36312,#36313,#36314,#36315,#36316,
#36317,#36318,#36319,#36320,#36321,#36322,#36323,#36324,#36325,#36326,#36327,
#36328,#36329,#36330,#36331,#36332,#36333,#36334,#36335,#36336,#36337,#36338,
#36339,#36340,#36341,#36342,#36343,#36344,#36345,#36346,#36347,#36348,#36349,
#36350,#36351,#36352,#36353,#36354,#36355,#36356,#36357,#36358,#36359,#36360,
#36361),.UNSPECIFIED.,.F.,.F.,(4,3,3,3,3,3,3,3,3,3,3,3,3,3,3,3,3,3,3,3,
3,3,3,3,3,3,3,3,3,3,3,3,3,3,3,3,3,3,3,3,3,3,3,3,3,3,3,3,3,3,3,3,3,3,3,3,
3,3,3,3,3,3,3,3,3,3,3,3,3,3,3,3,3,3,3,4),(311.017672705574,311.101135357737,
311.184495573409,311.267773766953,311.350990278642,311.434173266364,311.517340510539,
311.600510335937,311.683701065398,311.766980643786,311.850307293392,311.933762367981,
311.996907535779,312.080654268481,312.164297945497,312.247858689563,312.33135655152,
312.414819052082,312.498264187575,312.581710022418,312.665174617655,312.748727803077,
312.83232563665,312.916057199512,312.995891037979,313.079637770681,313.163281447697,
313.246842191764,313.33034005372,313.413802554283,313.497247689775,313.580693524618,
313.664158119856,313.747711305278,313.831309138851,313.915040701713,313.994874540178,
314.07862127288,314.162264949896,314.245825693962,314.329323555919,314.412786056481,
314.496231191973,314.579677026816,314.663141622054,314.746694807476,314.830292641049,
314.914024203911,314.993858042377,315.077604775079,315.161248452095,315.244809196161,
315.328307058118,315.41176955868,315.495214694172,315.578660529015,315.662125124253,
315.745678309675,315.829276143247,315.913007706109,315.992841544576,316.076588277278,
316.160231954294,316.24379269836,316.327290560316,316.410753060879,316.494198196372,
316.577644031215,316.661108626452,316.744661811874,316.828259645447,316.911991208309,
316.991825046775,317.092784210493,317.196821111451,317.30085801241),
 .UNSPECIFIED.);
#367=B_SPLINE_CURVE_WITH_KNOTS('',3,(#36363,#36364,#36365,#36366,#36367,
#36368,#36369,#36370,#36371,#36372,#36373,#36374,#36375,#36376,#36377,#36378,
#36379,#36380,#36381,#36382,#36383,#36384,#36385,#36386,#36387,#36388,#36389,
#36390,#36391,#36392,#36393,#36394,#36395,#36396,#36397,#36398,#36399,#36400,
#36401,#36402,#36403,#36404,#36405,#36406,#36407,#36408,#36409,#36410,#36411,
#36412,#36413,#36414,#36415,#36416,#36417,#36418,#36419,#36420,#36421,#36422,
#36423,#36424,#36425,#36426,#36427,#36428,#36429,#36430,#36431,#36432,#36433,
#36434,#36435,#36436,#36437,#36438,#36439,#36440,#36441,#36442,#36443,#36444,
#36445,#36446,#36447,#36448,#36449,#36450,#36451,#36452,#36453,#36454,#36455,
#36456,#36457,#36458,#36459,#36460,#36461,#36462,#36463,#36464,#36465,#36466,
#36467,#36468,#36469,#36470,#36471,#36472,#36473,#36474,#36475,#36476,#36477,
#36478,#36479,#36480,#36481,#36482,#36483,#36484,#36485,#36486,#36487,#36488,
#36489,#36490,#36491,#36492,#36493,#36494,#36495,#36496,#36497,#36498,#36499,
#36500,#36501,#36502,#36503,#36504,#36505,#36506,#36507,#36508,#36509,#36510,
#36511,#36512,#36513,#36514,#36515,#36516,#36517,#36518,#36519,#36520,#36521,
#36522,#36523,#36524,#36525,#36526,#36527,#36528,#36529,#36530,#36531,#36532,
#36533,#36534,#36535,#36536,#36537,#36538,#36539,#36540,#36541,#36542,#36543,
#36544,#36545,#36546,#36547,#36548,#36549,#36550,#36551,#36552,#36553,#36554,
#36555,#36556,#36557,#36558,#36559,#36560,#36561,#36562,#36563,#36564,#36565,
#36566,#36567,#36568,#36569,#36570,#36571,#36572,#36573,#36574,#36575,#36576,
#36577,#36578,#36579,#36580,#36581,#36582,#36583,#36584,#36585,#36586,#36587,
#36588,#36589,#36590,#36591),.UNSPECIFIED.,.F.,.F.,(4,3,3,3,3,3,3,3,3,3,
3,3,3,3,3,3,3,3,3,3,3,3,3,3,3,3,3,3,3,3,3,3,3,3,3,3,3,3,3,3,3,3,3,3,3,3,
3,3,3,3,3,3,3,3,3,3,3,3,3,3,3,3,3,3,3,3,3,3,3,3,3,3,3,3,3,3,4),(304.734487398388,
304.838750950482,304.944872023283,305.004023020385,305.087769753087,305.171413430103,
305.25497417417,305.338472036127,305.421934536689,305.505379672182,305.588825507025,
305.672290102263,305.755843287685,305.839441121258,305.92317268412,306.003006522584,
306.086753255286,306.170396932302,306.253957676368,306.337455538325,306.420918038888,
306.50436317438,306.587809009223,306.671273604461,306.754826789883,306.838424623456,
306.922156186318,307.001990024784,307.085736757486,307.169380434502,307.252941178568,
307.336439040525,307.419901541088,307.50334667658,307.586792511423,307.670257106661,
307.753810292083,307.837408125656,307.921139688518,308.000973526983,308.084720259685,
308.168363936701,308.251924680767,308.335422542724,308.418885043286,308.502330178779,
308.585776013621,308.669240608859,308.752793794281,308.836391627854,308.920123190716,
308.999957029182,309.083703761884,309.1673474389,309.250908182966,309.334406044923,
309.417868545485,309.501313680978,309.58475951582,309.668224111058,309.75177729648,
309.835375130053,309.919106692915,309.998940531381,310.082687264083,310.166330941099,
310.249891685165,310.333389547122,310.416852047684,310.500297183177,310.583743018019,
310.667207613257,310.750760798679,310.834358632252,310.918090195114,310.99792403358,
311.017672705391),.UNSPECIFIED.);
#368=B_SPLINE_CURVE_WITH_KNOTS('',3,(#36593,#36594,#36595,#36596,#36597,
#36598,#36599,#36600,#36601,#36602,#36603,#36604,#36605,#36606,#36607,#36608,
#36609,#36610,#36611,#36612,#36613,#36614,#36615,#36616,#36617,#36618,#36619,
#36620,#36621,#36622,#36623,#36624,#36625,#36626,#36627,#36628,#36629,#36630,
#36631,#36632,#36633,#36634,#36635,#36636,#36637,#36638,#36639,#36640,#36641,
#36642,#36643,#36644,#36645,#36646,#36647,#36648,#36649,#36650,#36651,#36652,
#36653,#36654,#36655,#36656,#36657,#36658,#36659,#36660,#36661,#36662,#36663,
#36664,#36665,#36666,#36667,#36668,#36669,#36670,#36671,#36672,#36673,#36674,
#36675,#36676,#36677,#36678,#36679,#36680,#36681,#36682,#36683,#36684,#36685,
#36686,#36687,#36688,#36689,#36690,#36691,#36692,#36693,#36694,#36695,#36696,
#36697,#36698,#36699,#36700,#36701,#36702,#36703,#36704,#36705,#36706,#36707,
#36708,#36709,#36710,#36711,#36712,#36713,#36714,#36715,#36716,#36717,#36718,
#36719,#36720,#36721,#36722,#36723,#36724,#36725,#36726,#36727,#36728,#36729,
#36730,#36731,#36732,#36733,#36734,#36735,#36736,#36737,#36738,#36739,#36740,
#36741,#36742,#36743,#36744,#36745,#36746,#36747,#36748,#36749,#36750,#36751,
#36752,#36753,#36754,#36755,#36756,#36757,#36758,#36759,#36760,#36761,#36762,
#36763,#36764,#36765,#36766,#36767,#36768,#36769,#36770,#36771,#36772,#36773,
#36774,#36775,#36776,#36777,#36778,#36779,#36780,#36781,#36782,#36783,#36784,
#36785,#36786,#36787,#36788,#36789,#36790,#36791,#36792,#36793,#36794,#36795,
#36796,#36797,#36798,#36799,#36800,#36801,#36802,#36803,#36804,#36805,#36806,
#36807,#36808,#36809,#36810,#36811,#36812,#36813,#36814,#36815,#36816,#36817,
#36818,#36819,#36820,#36821),.UNSPECIFIED.,.F.,.F.,(4,3,3,3,3,3,3,3,3,3,
3,3,3,3,3,3,3,3,3,3,3,3,3,3,3,3,3,3,3,3,3,3,3,3,3,3,3,3,3,3,3,3,3,3,3,3,
3,3,3,3,3,3,3,3,3,3,3,3,3,3,3,3,3,3,3,3,3,3,3,3,3,3,3,3,3,3,4),(298.451302091032,
298.536850673596,298.622451210915,298.708117991808,298.793927219197,298.879815482329,
298.965860496585,299.01012200719,299.093868739892,299.177512416908,299.261073160974,
299.344571022931,299.428033523493,299.511478658985,299.594924493828,299.678389089066,
299.761942274488,299.845540108061,299.929271670923,300.009105509389,300.092852242091,
300.176495919107,300.260056663173,300.34355452513,300.427017025693,300.510462161185,
300.593907996028,300.677372591266,300.760925776688,300.844523610261,300.928255173123,
301.008089011589,301.091835744291,301.175479421307,301.259040165374,301.342538027331,
301.426000527893,301.509445663386,301.592891498228,301.676356093467,301.759909278889,
301.843507112461,301.927238675323,302.007072513788,302.09081924649,302.174462923506,
302.258023667572,302.341521529529,302.424984030092,302.508429165584,302.591875000427,
302.675339595664,302.758892781086,302.842490614659,302.92622217752,303.006056015987,
303.089802748689,303.173446425705,303.257007169771,303.340505031727,303.42396753229,
303.507412667782,303.590858502625,303.674323097863,303.757876283285,303.841474116858,
303.925205679719,304.005039518186,304.087992711044,304.170814757054,304.253561341555,
304.336251293512,304.418903394483,304.501555863992,304.584205613442,304.666907824822,
304.734487398211),.UNSPECIFIED.);
#369=B_SPLINE_CURVE_WITH_KNOTS('',3,(#36823,#36824,#36825,#36826,#36827,
#36828,#36829,#36830,#36831,#36832,#36833,#36834,#36835,#36836,#36837,#36838,
#36839,#36840,#36841,#36842,#36843,#36844,#36845,#36846,#36847,#36848,#36849,
#36850,#36851,#36852,#36853,#36854,#36855,#36856,#36857,#36858,#36859,#36860,
#36861,#36862,#36863,#36864,#36865,#36866,#36867,#36868,#36869,#36870,#36871,
#36872,#36873,#36874,#36875,#36876,#36877,#36878,#36879,#36880,#36881,#36882,
#36883,#36884,#36885,#36886,#36887,#36888,#36889,#36890,#36891,#36892,#36893,
#36894,#36895,#36896,#36897,#36898,#36899,#36900,#36901,#36902,#36903,#36904,
#36905,#36906,#36907,#36908,#36909,#36910,#36911,#36912,#36913,#36914,#36915,
#36916,#36917,#36918,#36919,#36920,#36921,#36922,#36923,#36924,#36925,#36926,
#36927,#36928,#36929,#36930,#36931,#36932,#36933,#36934,#36935,#36936,#36937,
#36938,#36939,#36940,#36941,#36942,#36943,#36944,#36945,#36946,#36947,#36948,
#36949,#36950,#36951,#36952,#36953,#36954,#36955,#36956,#36957,#36958,#36959,
#36960,#36961,#36962,#36963,#36964,#36965,#36966,#36967,#36968,#36969,#36970,
#36971,#36972,#36973,#36974,#36975,#36976,#36977,#36978,#36979,#36980,#36981,
#36982,#36983,#36984,#36985,#36986,#36987,#36988,#36989,#36990,#36991,#36992,
#36993,#36994,#36995,#36996,#36997,#36998,#36999,#37000,#37001,#37002,#37003,
#37004,#37005,#37006,#37007,#37008,#37009,#37010,#37011,#37012,#37013,#37014,
#37015,#37016,#37017,#37018,#37019,#37020,#37021,#37022,#37023,#37024,#37025,
#37026,#37027,#37028,#37029,#37030,#37031,#37032,#37033,#37034,#37035,#37036,
#37037,#37038,#37039,#37040,#37041,#37042,#37043,#37044,#37045,#37046,#37047,
#37048,#37049,#37050,#37051),.UNSPECIFIED.,.F.,.F.,(4,3,3,3,3,3,3,3,3,3,
3,3,3,3,3,3,3,3,3,3,3,3,3,3,3,3,3,3,3,3,3,3,3,3,3,3,3,3,3,3,3,3,3,3,3,3,
3,3,3,3,3,3,3,3,3,3,3,3,3,3,3,3,3,3,3,3,3,3,3,3,3,3,3,3,3,3,4),(292.168116783963,
292.250528923154,292.332859281583,292.418279495635,292.500516709425,292.582741209567,
292.664972016471,292.747228153625,292.829572299424,292.911968827067,292.994480032763,
293.016220993995,293.099967726697,293.183611403713,293.267172147779,293.350670009736,
293.434132510299,293.517577645791,293.601023480634,293.684488075872,293.768041261294,
293.851639094867,293.935370657729,294.015204496194,294.098951228896,294.182594905912,
294.266155649978,294.349653511935,294.433116012497,294.51656114799,294.600006982832,
294.68347157807,294.767024763492,294.850622597065,294.934354159927,295.014187998394,
295.097934731096,295.181578408112,295.265139152179,295.348637014135,295.432099514698,
295.51554465019,295.598990485033,295.682455080272,295.766008265694,295.849606099267,
295.933337662129,296.013171500593,296.096918233295,296.180561910311,296.264122654377,
296.347620516334,296.431083016896,296.514528152388,296.597973987231,296.681438582469,
296.76499176789,296.848589601463,296.932321164325,297.012155002792,297.095901735494,
297.17954541251,297.263106156576,297.346604018533,297.430066519095,297.513511654588,
297.59695748943,297.680422084669,297.76397527009,297.847573103663,297.931304666525,
298.011138504991,298.10192502492,298.192405175669,298.282698199155,298.372692110768,
298.451302090907),.UNSPECIFIED.);
#370=B_SPLINE_CURVE_WITH_KNOTS('',3,(#37053,#37054,#37055,#37056,#37057,
#37058,#37059,#37060,#37061,#37062,#37063,#37064,#37065,#37066,#37067,#37068,
#37069,#37070,#37071,#37072,#37073,#37074,#37075,#37076,#37077,#37078,#37079,
#37080,#37081,#37082,#37083,#37084,#37085,#37086,#37087,#37088,#37089,#37090,
#37091,#37092,#37093,#37094,#37095,#37096,#37097,#37098,#37099,#37100,#37101,
#37102,#37103,#37104,#37105,#37106,#37107,#37108,#37109,#37110,#37111,#37112,
#37113,#37114,#37115,#37116,#37117,#37118,#37119,#37120,#37121,#37122,#37123,
#37124,#37125,#37126,#37127,#37128,#37129,#37130,#37131,#37132,#37133,#37134,
#37135,#37136,#37137,#37138,#37139,#37140,#37141,#37142,#37143,#37144,#37145,
#37146,#37147,#37148,#37149,#37150,#37151,#37152,#37153,#37154,#37155,#37156,
#37157,#37158,#37159,#37160,#37161,#37162,#37163,#37164,#37165,#37166,#37167,
#37168,#37169,#37170,#37171,#37172,#37173,#37174,#37175,#37176,#37177,#37178,
#37179,#37180,#37181,#37182,#37183,#37184,#37185,#37186,#37187,#37188,#37189,
#37190,#37191,#37192,#37193,#37194,#37195,#37196,#37197,#37198,#37199,#37200,
#37201,#37202,#37203,#37204,#37205,#37206,#37207,#37208,#37209,#37210,#37211,
#37212,#37213,#37214,#37215,#37216,#37217,#37218,#37219,#37220,#37221,#37222,
#37223,#37224,#37225,#37226,#37227,#37228,#37229,#37230,#37231,#37232,#37233,
#37234,#37235,#37236,#37237,#37238,#37239,#37240,#37241,#37242,#37243,#37244,
#37245,#37246,#37247,#37248,#37249,#37250,#37251,#37252,#37253,#37254,#37255,
#37256,#37257,#37258,#37259,#37260,#37261,#37262,#37263,#37264,#37265,#37266,
#37267,#37268,#37269,#37270,#37271,#37272,#37273,#37274,#37275,#37276,#37277,
#37278),.UNSPECIFIED.,.F.,.F.,(4,3,3,3,3,3,3,3,3,3,3,3,3,3,3,3,3,3,3,3,
3,3,3,3,3,3,3,3,3,3,3,3,3,3,3,3,3,3,3,3,3,3,3,3,3,3,3,3,3,3,3,3,3,3,3,3,
3,3,3,3,3,3,3,3,3,3,3,3,3,3,3,3,3,3,3,4),(285.884931476672,286.023336478601,
286.107083211303,286.190726888319,286.274287632385,286.357785494342,286.441247994905,
286.524693130397,286.60813896524,286.691603560478,286.7751567459,286.858754579472,
286.942486142334,287.0223199808,287.106066713502,287.189710390518,287.273271134584,
287.356768996541,287.440231497104,287.523676632596,287.607122467439,287.690587062677,
287.774140248099,287.857738081671,287.941469644533,288.021303482999,288.105050215701,
288.188693892717,288.272254636783,288.35575249874,288.439214999303,288.522660134795,
288.606105969638,288.689570564876,288.773123750298,288.85672158387,288.940453146732,
289.020286985199,289.104033717901,289.187677394917,289.271238138984,289.35473600094,
289.438198501503,289.521643636995,289.605089471838,289.688554067076,289.772107252498,
289.855705086071,289.939436648933,290.019270487398,290.1030172201,290.186660897116,
290.270221641182,290.353719503139,290.437182003701,290.520627139194,290.604072974037,
290.687537569275,290.771090754697,290.854688588269,290.938420151131,291.018253989597,
291.102000722299,291.185644399315,291.269205143381,291.352703005338,291.4361655059,
291.519610641392,291.603056476235,291.686521071473,291.770074256895,291.853672090467,
291.937403653329,292.017237491796,292.158686771192,292.168116783852),
 .UNSPECIFIED.);
#371=B_SPLINE_CURVE_WITH_KNOTS('',3,(#37280,#37281,#37282,#37283,#37284,
#37285,#37286,#37287,#37288,#37289,#37290,#37291,#37292,#37293,#37294,#37295,
#37296,#37297,#37298,#37299,#37300,#37301,#37302,#37303,#37304,#37305,#37306,
#37307,#37308,#37309,#37310,#37311,#37312,#37313,#37314,#37315,#37316,#37317,
#37318,#37319,#37320,#37321,#37322,#37323,#37324,#37325,#37326,#37327,#37328,
#37329,#37330,#37331,#37332,#37333,#37334,#37335,#37336,#37337,#37338,#37339,
#37340,#37341,#37342,#37343,#37344,#37345,#37346,#37347,#37348,#37349,#37350,
#37351,#37352,#37353,#37354,#37355,#37356,#37357,#37358,#37359,#37360,#37361,
#37362,#37363,#37364,#37365,#37366,#37367,#37368,#37369,#37370,#37371,#37372,
#37373,#37374,#37375,#37376,#37377,#37378,#37379,#37380,#37381,#37382,#37383,
#37384,#37385,#37386,#37387,#37388,#37389,#37390,#37391,#37392,#37393,#37394,
#37395,#37396,#37397,#37398,#37399,#37400,#37401,#37402,#37403,#37404,#37405,
#37406,#37407,#37408,#37409,#37410,#37411,#37412,#37413,#37414,#37415,#37416,
#37417,#37418,#37419,#37420,#37421,#37422,#37423,#37424,#37425,#37426,#37427,
#37428,#37429,#37430,#37431,#37432,#37433,#37434,#37435,#37436,#37437,#37438,
#37439,#37440,#37441,#37442,#37443,#37444,#37445,#37446,#37447,#37448,#37449,
#37450,#37451,#37452,#37453,#37454,#37455,#37456,#37457,#37458,#37459,#37460,
#37461,#37462,#37463,#37464,#37465,#37466,#37467,#37468,#37469,#37470,#37471,
#37472,#37473,#37474,#37475,#37476,#37477,#37478,#37479,#37480,#37481,#37482,
#37483,#37484,#37485,#37486,#37487,#37488,#37489,#37490,#37491,#37492,#37493,
#37494,#37495,#37496,#37497,#37498,#37499,#37500,#37501,#37502,#37503,#37504,
#37505,#37506,#37507,#37508),.UNSPECIFIED.,.F.,.F.,(4,3,3,3,3,3,3,3,3,3,
3,3,3,3,3,3,3,3,3,3,3,3,3,3,3,3,3,3,3,3,3,3,3,3,3,3,3,3,3,3,3,3,3,3,3,3,
3,3,3,3,3,3,3,3,3,3,3,3,3,3,3,3,3,3,3,3,3,3,3,3,3,3,3,3,3,3,4),(279.601746169493,
279.692274093846,279.783190578907,279.874304142487,279.965719750968,280.029435465406,
280.113182198108,280.196825875124,280.28038661919,280.363884481147,280.447346981709,
280.530792117201,280.614237952044,280.697702547282,280.781255732704,280.864853566276,
280.948585129138,281.028418967605,281.112165700307,281.195809377323,281.279370121389,
281.362867983346,281.446330483909,281.529775619401,281.613221454244,281.696686049482,
281.780239234904,281.863837068477,281.947568631339,282.027402469804,282.111149202506,
282.194792879522,282.278353623588,282.361851485545,282.445313986108,282.5287591216,
282.612204956443,282.695669551681,282.779222737103,282.862820570676,282.946552133538,
283.026385972004,283.110132704706,283.193776381722,283.277337125788,283.360834987745,
283.444297488308,283.5277426238,283.611188458643,283.694653053881,283.778206239303,
283.861804072876,283.945535635738,284.025369474203,284.109116206905,284.192759883921,
284.276320627987,284.359818489944,284.443280990507,284.526726125999,284.610171960842,
284.69363655608,284.777189741502,284.860787575074,284.944519137936,285.024352976402,
285.106888703548,285.189322170556,285.271674581163,285.353965488497,285.436224067443,
285.518469335565,285.600720296674,285.683033431969,285.765381886047,285.847828289346,
285.88493147655),.UNSPECIFIED.);
#372=B_SPLINE_CURVE_WITH_KNOTS('',3,(#37510,#37511,#37512,#37513,#37514,
#37515,#37516,#37517,#37518,#37519),.UNSPECIFIED.,.F.,.F.,(4,1,1,1,1,1,
1,4),(273.318560862313,274.035534452211,275.03451795441,276.033501456609,
277.032484958809,278.031468461008,279.030451963207,279.601746169493),
 .UNSPECIFIED.);
#373=B_SPLINE_CURVE_WITH_KNOTS('',3,(#37521,#37522,#37523,#37524,#37525,
#37526,#37527,#37528,#37529,#37530,#37531,#37532,#37533,#37534,#37535,#37536,
#37537,#37538,#37539,#37540,#37541,#37542,#37543,#37544,#37545,#37546,#37547,
#37548,#37549,#37550,#37551,#37552,#37553,#37554,#37555,#37556,#37557,#37558,
#37559,#37560,#37561,#37562,#37563,#37564,#37565,#37566,#37567,#37568,#37569,
#37570,#37571,#37572,#37573,#37574,#37575,#37576,#37577,#37578,#37579,#37580,
#37581,#37582,#37583,#37584,#37585,#37586,#37587,#37588,#37589,#37590,#37591,
#37592,#37593,#37594,#37595,#37596,#37597,#37598,#37599,#37600,#37601,#37602,
#37603,#37604,#37605,#37606,#37607,#37608,#37609,#37610,#37611,#37612,#37613,
#37614,#37615,#37616,#37617,#37618,#37619,#37620,#37621,#37622,#37623,#37624,
#37625,#37626,#37627,#37628,#37629,#37630,#37631,#37632,#37633,#37634,#37635,
#37636,#37637,#37638,#37639,#37640,#37641,#37642,#37643,#37644,#37645,#37646,
#37647,#37648,#37649,#37650,#37651,#37652,#37653,#37654,#37655,#37656,#37657,
#37658,#37659,#37660,#37661,#37662,#37663,#37664,#37665,#37666,#37667,#37668,
#37669,#37670,#37671,#37672,#37673,#37674,#37675,#37676,#37677,#37678,#37679,
#37680,#37681,#37682,#37683,#37684,#37685,#37686,#37687,#37688,#37689,#37690,
#37691,#37692,#37693,#37694,#37695,#37696,#37697,#37698,#37699,#37700,#37701,
#37702,#37703,#37704,#37705,#37706,#37707,#37708,#37709,#37710,#37711,#37712,
#37713,#37714,#37715,#37716,#37717,#37718,#37719,#37720,#37721,#37722,#37723,
#37724,#37725,#37726,#37727,#37728,#37729,#37730,#37731,#37732,#37733,#37734,
#37735,#37736,#37737,#37738,#37739,#37740,#37741,#37742,#37743,#37744,#37745,
#37746,#37747,#37748,#37749),.UNSPECIFIED.,.F.,.F.,(4,3,3,3,3,3,3,3,3,3,
3,3,3,3,3,3,3,3,3,3,3,3,3,3,3,3,3,3,3,3,3,3,3,3,3,3,3,3,3,3,3,3,3,3,3,3,
3,3,3,3,3,3,3,3,3,3,3,3,3,3,3,3,3,3,3,3,3,3,3,3,3,3,3,3,3,3,4),(267.035375555134,
267.042649936817,267.126396669519,267.210040346535,267.293601090601,267.377098952558,
267.460561453121,267.544006588613,267.627452423456,267.710917018694,267.794470204116,
267.878068037689,267.961799600551,268.041633439016,268.125380171718,268.209023848734,
268.2925845928,268.376082454757,268.45954495532,268.542990090812,268.626435925655,
268.709900520893,268.793453706314,268.877051539887,268.960783102749,269.040616941215,
269.124363673917,269.208007350933,269.291568094999,269.375065956956,269.458528457519,
269.541973593011,269.625419427854,269.708884023092,269.792437208514,269.876035042087,
269.959766604949,270.039600443414,270.123347176116,270.206990853132,270.290551597198,
270.374049459155,270.457511959718,270.54095709521,270.624402930053,270.707867525291,
270.791420710713,270.875018544286,270.958750107147,271.038583945614,271.122330678316,
271.205974355332,271.289535099398,271.373032961355,271.456495461918,271.53994059741,
271.623386432253,271.706851027491,271.790404212913,271.874002046486,271.957733609348,
272.037567447813,272.121314180515,272.204957857531,272.288518601597,272.372016463554,
272.455478964116,272.538924099609,272.622369934452,272.70583452969,272.789387715111,
272.872985548684,272.956717111546,273.036550950012,273.140987376872,273.243878527479,
273.318560862313),.UNSPECIFIED.);
#374=B_SPLINE_CURVE_WITH_KNOTS('',3,(#37751,#37752,#37753,#37754,#37755,
#37756,#37757,#37758,#37759,#37760,#37761,#37762,#37763,#37764,#37765,#37766,
#37767,#37768,#37769,#37770,#37771,#37772,#37773,#37774,#37775,#37776,#37777,
#37778,#37779,#37780,#37781,#37782,#37783,#37784,#37785,#37786,#37787,#37788,
#37789,#37790,#37791,#37792,#37793,#37794,#37795,#37796,#37797,#37798,#37799,
#37800,#37801,#37802,#37803,#37804,#37805,#37806,#37807,#37808,#37809,#37810,
#37811,#37812,#37813,#37814,#37815,#37816,#37817,#37818,#37819,#37820,#37821,
#37822,#37823,#37824,#37825,#37826,#37827,#37828,#37829,#37830,#37831,#37832,
#37833,#37834,#37835,#37836,#37837,#37838,#37839,#37840,#37841,#37842,#37843,
#37844,#37845,#37846,#37847,#37848,#37849,#37850,#37851,#37852,#37853,#37854,
#37855,#37856,#37857,#37858,#37859,#37860,#37861,#37862,#37863,#37864,#37865,
#37866,#37867,#37868,#37869,#37870,#37871,#37872,#37873,#37874,#37875,#37876,
#37877,#37878,#37879,#37880,#37881,#37882,#37883,#37884,#37885,#37886,#37887,
#37888,#37889,#37890,#37891,#37892,#37893,#37894,#37895,#37896,#37897,#37898,
#37899,#37900,#37901,#37902,#37903,#37904,#37905,#37906,#37907,#37908,#37909,
#37910,#37911,#37912,#37913,#37914,#37915,#37916,#37917,#37918,#37919,#37920,
#37921,#37922,#37923,#37924,#37925,#37926,#37927,#37928,#37929,#37930,#37931,
#37932,#37933,#37934,#37935,#37936,#37937,#37938,#37939,#37940,#37941,#37942,
#37943,#37944,#37945,#37946,#37947,#37948,#37949,#37950,#37951,#37952,#37953,
#37954,#37955,#37956,#37957,#37958,#37959,#37960,#37961,#37962,#37963,#37964,
#37965,#37966,#37967,#37968,#37969,#37970,#37971,#37972,#37973,#37974,#37975,
#37976),.UNSPECIFIED.,.F.,.F.,(4,3,3,3,3,3,3,3,3,3,3,3,3,3,3,3,3,3,3,3,
3,3,3,3,3,3,3,3,3,3,3,3,3,3,3,3,3,3,3,3,3,3,3,3,3,3,3,3,3,3,3,3,3,3,3,3,
3,3,3,3,3,3,3,3,3,3,3,3,3,3,3,3,3,3,3,4),(260.752190248095,260.853081327826,
260.955336834719,261.048748923622,261.132495656324,261.21613933334,261.299700077406,
261.383197939363,261.466660439926,261.550105575418,261.633551410261,261.717016005499,
261.80056919092,261.884167024493,261.967898587355,262.047732425821,262.131479158523,
262.215122835539,262.298683579605,262.382181441562,262.465643942124,262.549089077617,
262.632534912459,262.715999507697,262.799552693119,262.883150526692,262.966882089554,
263.04671592802,263.130462660722,263.214106337738,263.297667081804,263.381164943761,
263.464627444324,263.548072579816,263.631518414659,263.714983009897,263.798536195319,
263.882134028891,263.965865591753,264.045699430219,264.129446162921,264.213089839937,
264.296650584003,264.38014844596,264.463610946523,264.547056082015,264.630501916858,
264.713966512096,264.797519697518,264.881117531091,264.964849093953,265.044682932419,
265.128429665121,265.212073342137,265.295634086204,265.37913194816,265.462594448723,
265.546039584215,265.629485419058,265.712950014296,265.796503199718,265.880101033291,
265.963832596153,266.043666434618,266.127304946033,266.2108404585,266.294293211055,
266.377683369963,266.461038639883,266.544377018387,266.627716673381,266.711075769832,
266.794523426635,266.878016543539,266.961641353193,267.035375554993),
 .UNSPECIFIED.);
#375=B_SPLINE_CURVE_WITH_KNOTS('',3,(#37978,#37979,#37980,#37981,#37982,
#37983,#37984,#37985,#37986,#37987,#37988,#37989,#37990,#37991,#37992,#37993,
#37994,#37995,#37996,#37997,#37998,#37999,#38000,#38001,#38002,#38003,#38004,
#38005,#38006,#38007,#38008,#38009,#38010,#38011,#38012,#38013,#38014,#38015,
#38016,#38017,#38018,#38019,#38020,#38021,#38022,#38023,#38024,#38025,#38026,
#38027,#38028,#38029,#38030,#38031,#38032,#38033,#38034,#38035,#38036,#38037,
#38038,#38039,#38040,#38041,#38042,#38043,#38044,#38045,#38046,#38047,#38048,
#38049,#38050,#38051,#38052,#38053,#38054,#38055,#38056,#38057,#38058,#38059,
#38060,#38061,#38062,#38063,#38064,#38065,#38066,#38067,#38068,#38069,#38070,
#38071,#38072,#38073,#38074,#38075,#38076,#38077,#38078,#38079,#38080,#38081,
#38082,#38083,#38084,#38085,#38086,#38087,#38088,#38089,#38090,#38091,#38092,
#38093,#38094,#38095,#38096,#38097,#38098,#38099,#38100,#38101,#38102,#38103,
#38104,#38105,#38106,#38107,#38108,#38109,#38110,#38111,#38112,#38113,#38114,
#38115,#38116,#38117,#38118,#38119,#38120,#38121,#38122,#38123,#38124,#38125,
#38126,#38127,#38128,#38129,#38130,#38131,#38132,#38133,#38134,#38135,#38136,
#38137,#38138,#38139,#38140,#38141,#38142,#38143,#38144,#38145,#38146,#38147,
#38148,#38149,#38150,#38151,#38152,#38153,#38154,#38155,#38156,#38157,#38158,
#38159,#38160,#38161,#38162,#38163,#38164,#38165,#38166,#38167,#38168,#38169,
#38170,#38171,#38172,#38173,#38174,#38175,#38176,#38177,#38178,#38179,#38180,
#38181,#38182,#38183,#38184,#38185,#38186,#38187,#38188,#38189,#38190,#38191,
#38192,#38193,#38194,#38195,#38196,#38197,#38198,#38199,#38200,#38201,#38202,
#38203,#38204,#38205,#38206),.UNSPECIFIED.,.F.,.F.,(4,3,3,3,3,3,3,3,3,3,
3,3,3,3,3,3,3,3,3,3,3,3,3,3,3,3,3,3,3,3,3,3,3,3,3,3,3,3,3,3,3,3,3,3,3,3,
3,3,3,3,3,3,3,3,3,3,3,3,3,3,3,3,3,3,3,3,3,3,3,3,3,3,3,3,3,3,4),(254.469004940775,
254.553878218561,254.638782764637,254.723734366107,254.808811034956,254.893952704628,
254.979252035181,255.054847910427,255.138594643129,255.222238320145,255.305799064211,
255.389296926168,255.47275942673,255.556204562223,255.639650397065,255.723114992303,
255.806668177725,255.890266011298,255.97399757416,256.053831412626,256.137578145328,
256.221221822344,256.30478256641,256.388280428367,256.47174292893,256.555188064422,
256.638633899265,256.722098494503,256.805651679925,256.889249513498,256.97298107636,
257.052814914825,257.136561647527,257.220205324543,257.303766068609,257.387263930566,
257.470726431129,257.554171566621,257.637617401464,257.721081996702,257.804635182123,
257.888233015696,257.971964578558,258.051798417024,258.135545149726,258.219188826742,
258.302749570808,258.386247432765,258.469709933328,258.55315506882,258.636600903663,
258.720065498901,258.803618684323,258.887216517896,258.970948080758,259.050781919224,
259.134528651926,259.218172328942,259.301733073008,259.385230934965,259.468693435527,
259.55213857102,259.635584405862,259.7190490011,259.802602186522,259.886200020095,
259.969931582957,260.049765421423,260.133000554424,260.216101211117,260.299124012296,
260.38208757138,260.465010454567,260.547924974296,260.630834260175,260.713780358084,
260.752190247954),.UNSPECIFIED.);
#376=B_SPLINE_CURVE_WITH_KNOTS('',3,(#38208,#38209,#38210,#38211,#38212,
#38213,#38214,#38215,#38216,#38217,#38218,#38219,#38220,#38221,#38222,#38223,
#38224,#38225,#38226,#38227,#38228,#38229,#38230,#38231,#38232,#38233,#38234,
#38235,#38236,#38237,#38238,#38239,#38240,#38241,#38242,#38243,#38244,#38245,
#38246,#38247,#38248,#38249,#38250,#38251,#38252,#38253,#38254,#38255,#38256,
#38257,#38258,#38259,#38260,#38261,#38262,#38263,#38264,#38265,#38266,#38267,
#38268,#38269,#38270,#38271,#38272,#38273,#38274,#38275,#38276,#38277,#38278,
#38279,#38280,#38281,#38282,#38283,#38284,#38285,#38286,#38287,#38288,#38289,
#38290,#38291,#38292,#38293,#38294,#38295,#38296,#38297,#38298,#38299,#38300,
#38301,#38302,#38303,#38304,#38305,#38306,#38307,#38308,#38309,#38310,#38311,
#38312,#38313,#38314,#38315,#38316,#38317,#38318,#38319,#38320,#38321,#38322,
#38323,#38324,#38325,#38326,#38327,#38328,#38329,#38330,#38331,#38332,#38333,
#38334,#38335,#38336,#38337,#38338,#38339,#38340,#38341,#38342,#38343,#38344,
#38345,#38346,#38347,#38348,#38349,#38350,#38351,#38352,#38353,#38354,#38355,
#38356,#38357,#38358,#38359,#38360,#38361,#38362,#38363,#38364,#38365,#38366,
#38367,#38368,#38369,#38370,#38371,#38372,#38373,#38374,#38375,#38376,#38377,
#38378,#38379,#38380,#38381,#38382,#38383,#38384,#38385,#38386,#38387,#38388,
#38389,#38390,#38391,#38392,#38393,#38394,#38395,#38396,#38397,#38398,#38399,
#38400,#38401,#38402,#38403,#38404,#38405,#38406,#38407,#38408,#38409,#38410,
#38411,#38412,#38413,#38414,#38415,#38416,#38417,#38418,#38419,#38420,#38421,
#38422,#38423,#38424,#38425,#38426,#38427,#38428,#38429,#38430,#38431,#38432,
#38433,#38434,#38435,#38436),.UNSPECIFIED.,.F.,.F.,(4,3,3,3,3,3,3,3,3,3,
3,3,3,3,3,3,3,3,3,3,3,3,3,3,3,3,3,3,3,3,3,3,3,3,3,3,3,3,3,3,3,3,3,3,3,3,
3,3,3,3,3,3,3,3,3,3,3,3,3,3,3,3,3,3,3,3,3,3,3,3,3,3,3,3,3,3,4),(248.185819633726,
248.268331196131,248.350754928891,248.433111935712,248.515429379703,248.597727820277,
248.680026236115,248.762343603558,248.844746147529,248.927195249346,249.009767054777,
249.060946897232,249.144693629934,249.22833730695,249.311898051016,249.395395912973,
249.478858413536,249.562303549028,249.645749383871,249.729213979109,249.812767164531,
249.896364998103,249.980096560965,250.059930399431,250.143677132133,250.227320809149,
250.310881553215,250.394379415172,250.477841915734,250.561287051227,250.64473288607,
250.728197481308,250.811750666729,250.895348500302,250.979080063164,251.05891390163,
251.142660634332,251.226304311348,251.309865055414,251.393362917371,251.476825417934,
251.560270553426,251.643716388268,251.727180983507,251.810734168929,251.894332002501,
251.978063565363,252.057897403829,252.141644136531,252.225287813547,252.308848557614,
252.392346419571,252.475808920134,252.559254055626,252.642699890469,252.726164485707,
252.809717671128,252.893315504701,252.977047067563,253.056880906029,253.140627638731,
253.224271315746,253.307832059813,253.39132992177,253.474792422332,253.558237557825,
253.641683392668,253.725147987906,253.808701173327,253.8922990069,253.976030569762,
254.055864408228,254.148202186826,254.240178487622,254.331921438503,254.42329568607,
254.46900494061),.UNSPECIFIED.);
#377=B_SPLINE_CURVE_WITH_KNOTS('',3,(#38438,#38439,#38440,#38441,#38442,
#38443,#38444,#38445,#38446,#38447,#38448,#38449,#38450,#38451,#38452,#38453,
#38454,#38455,#38456,#38457,#38458,#38459,#38460,#38461,#38462,#38463,#38464,
#38465,#38466,#38467,#38468,#38469,#38470,#38471,#38472,#38473,#38474,#38475,
#38476,#38477,#38478,#38479,#38480,#38481,#38482,#38483,#38484,#38485,#38486,
#38487,#38488,#38489,#38490,#38491,#38492,#38493,#38494,#38495,#38496,#38497,
#38498,#38499,#38500,#38501,#38502,#38503,#38504,#38505,#38506,#38507,#38508,
#38509,#38510,#38511,#38512,#38513,#38514,#38515,#38516,#38517,#38518,#38519,
#38520,#38521,#38522,#38523,#38524,#38525,#38526,#38527,#38528,#38529,#38530,
#38531,#38532,#38533,#38534,#38535,#38536,#38537,#38538,#38539,#38540,#38541,
#38542,#38543,#38544,#38545,#38546,#38547,#38548,#38549,#38550,#38551,#38552,
#38553,#38554,#38555,#38556,#38557,#38558,#38559,#38560,#38561,#38562,#38563,
#38564,#38565,#38566,#38567,#38568,#38569,#38570,#38571,#38572,#38573,#38574,
#38575,#38576,#38577,#38578,#38579,#38580,#38581,#38582,#38583,#38584,#38585,
#38586,#38587,#38588,#38589,#38590,#38591,#38592,#38593,#38594,#38595,#38596,
#38597,#38598,#38599,#38600,#38601,#38602,#38603,#38604,#38605,#38606,#38607,
#38608,#38609,#38610,#38611,#38612,#38613,#38614,#38615,#38616,#38617,#38618,
#38619,#38620,#38621,#38622,#38623,#38624,#38625,#38626,#38627,#38628,#38629,
#38630,#38631,#38632,#38633,#38634,#38635,#38636,#38637,#38638,#38639,#38640,
#38641,#38642,#38643,#38644,#38645,#38646,#38647,#38648,#38649,#38650,#38651,
#38652,#38653,#38654,#38655,#38656,#38657,#38658,#38659,#38660,#38661,#38662,
#38663),.UNSPECIFIED.,.F.,.F.,(4,3,3,3,3,3,3,3,3,3,3,3,3,3,3,3,3,3,3,3,
3,3,3,3,3,3,3,3,3,3,3,3,3,3,3,3,3,3,3,3,3,3,3,3,3,3,3,3,3,3,3,3,3,3,3,3,
3,3,3,3,3,3,3,3,3,3,3,3,3,3,3,3,3,3,3,4),(241.902634326415,242.036118860327,
242.068062381838,242.15180911454,242.235452791556,242.319013535622,242.402511397579,
242.485973898142,242.569419033634,242.652864868477,242.736329463715,242.819882649137,
242.903480482709,242.987212045571,243.067045884037,243.150792616739,243.234436293755,
243.317997037821,243.401494899778,243.48495740034,243.568402535833,243.651848370675,
243.735312965913,243.818866151335,243.902463984908,243.98619554777,244.066029386236,
244.149776118938,244.233419795954,244.31698054002,244.400478401977,244.483940902539,
244.567386038032,244.650831872874,244.734296468112,244.817849653534,244.901447487107,
244.985179049969,245.065012888435,245.148759621137,245.232403298153,245.315964042219,
245.399461904176,245.482924404739,245.566369540231,245.649815375074,245.733279970312,
245.816833155734,245.900430989307,245.984162552168,246.063996390634,246.147743123336,
246.231386800352,246.314947544418,246.398445406375,246.481907906938,246.56535304243,
246.648798877273,246.732263472511,246.815816657933,246.899414491506,246.983146054368,
247.062979892834,247.146726625536,247.230370302552,247.313931046619,247.397428908575,
247.480891409138,247.56433654463,247.647782379473,247.731246974711,247.814800160133,
247.898397993706,247.982129556568,248.061963395033,248.185819633595),
 .UNSPECIFIED.);
#378=B_SPLINE_CURVE_WITH_KNOTS('',3,(#38665,#38666,#38667,#38668,#38669,
#38670,#38671,#38672,#38673,#38674,#38675,#38676,#38677,#38678,#38679,#38680,
#38681,#38682,#38683,#38684,#38685,#38686,#38687,#38688,#38689,#38690,#38691,
#38692,#38693,#38694,#38695,#38696,#38697,#38698,#38699,#38700,#38701,#38702,
#38703,#38704,#38705,#38706,#38707,#38708,#38709,#38710,#38711,#38712,#38713,
#38714,#38715,#38716,#38717,#38718,#38719,#38720,#38721,#38722,#38723,#38724,
#38725,#38726,#38727,#38728,#38729,#38730,#38731,#38732,#38733,#38734,#38735,
#38736,#38737,#38738,#38739,#38740,#38741,#38742,#38743,#38744,#38745,#38746,
#38747,#38748,#38749,#38750,#38751,#38752,#38753,#38754,#38755,#38756,#38757,
#38758,#38759,#38760,#38761,#38762,#38763,#38764,#38765,#38766,#38767,#38768,
#38769,#38770,#38771,#38772,#38773,#38774,#38775,#38776,#38777,#38778,#38779,
#38780,#38781,#38782,#38783,#38784,#38785,#38786,#38787,#38788,#38789,#38790,
#38791,#38792,#38793,#38794,#38795,#38796,#38797,#38798,#38799,#38800,#38801,
#38802,#38803,#38804,#38805,#38806,#38807,#38808,#38809,#38810,#38811,#38812,
#38813,#38814,#38815,#38816,#38817,#38818,#38819,#38820,#38821,#38822,#38823,
#38824,#38825,#38826,#38827,#38828,#38829,#38830,#38831,#38832,#38833,#38834,
#38835,#38836,#38837,#38838,#38839,#38840,#38841,#38842,#38843,#38844,#38845,
#38846,#38847,#38848,#38849,#38850,#38851,#38852,#38853,#38854,#38855,#38856,
#38857,#38858,#38859,#38860,#38861,#38862,#38863,#38864,#38865,#38866,#38867,
#38868,#38869,#38870,#38871,#38872,#38873,#38874,#38875,#38876,#38877,#38878,
#38879,#38880,#38881,#38882,#38883,#38884,#38885,#38886,#38887,#38888,#38889,
#38890),.UNSPECIFIED.,.F.,.F.,(4,3,3,3,3,3,3,3,3,3,3,3,3,3,3,3,3,3,3,3,
3,3,3,3,3,3,3,3,3,3,3,3,3,3,3,3,3,3,3,3,3,3,3,3,3,3,3,3,3,3,3,3,3,3,3,3,
3,3,3,3,3,3,3,3,3,3,3,3,3,3,3,3,3,3,3,4),(235.619449019423,235.70867099603,
235.800043589183,235.889734382521,235.981947875582,236.074161368643,236.157908101345,
236.241551778361,236.325112522427,236.408610384384,236.492072884947,236.575518020439,
236.658963855282,236.74242845052,236.825981635942,236.909579469515,236.993311032377,
237.073144870842,237.156891603544,237.24053528056,237.324096024626,237.407593886583,
237.491056387145,237.574501522638,237.65794735748,237.741411952719,237.82496513814,
237.908562971713,237.992294534575,238.072128373041,238.155875105743,238.239518782759,
238.323079526825,238.406577388782,238.490039889344,238.573485024837,238.656930859679,
238.740395454917,238.823948640339,238.907546473912,238.991278036774,239.07111187524,
239.154858607942,239.238502284958,239.322063029024,239.405560890981,239.489023391544,
239.572468527036,239.655914361879,239.739378957117,239.822932142539,239.906529976112,
239.990261538974,240.070095377439,240.153842110141,240.237485787157,240.321046531223,
240.40454439318,240.488006893743,240.571452029235,240.654897864078,240.738362459316,
240.821915644738,240.90551347831,240.989245041172,241.069078879639,241.151576682586,
241.233971985748,241.317554778307,241.399805543854,241.482023949524,241.564229036275,
241.648830358762,241.731098704372,241.816866515298,241.902634326224),
 .UNSPECIFIED.);
#379=B_SPLINE_CURVE_WITH_KNOTS('',3,(#38892,#38893,#38894,#38895,#38896,
#38897,#38898,#38899,#38900,#38901,#38902,#38903,#38904,#38905,#38906,#38907,
#38908,#38909,#38910,#38911,#38912,#38913,#38914,#38915,#38916,#38917,#38918,
#38919,#38920,#38921,#38922,#38923,#38924,#38925,#38926,#38927,#38928,#38929,
#38930,#38931,#38932,#38933,#38934,#38935,#38936,#38937,#38938,#38939,#38940,
#38941,#38942,#38943,#38944,#38945,#38946,#38947,#38948,#38949,#38950,#38951,
#38952,#38953,#38954,#38955,#38956,#38957,#38958,#38959,#38960,#38961,#38962,
#38963,#38964,#38965,#38966,#38967,#38968,#38969,#38970,#38971,#38972,#38973,
#38974,#38975,#38976,#38977,#38978,#38979,#38980,#38981,#38982,#38983,#38984,
#38985,#38986,#38987,#38988,#38989,#38990,#38991,#38992,#38993,#38994,#38995,
#38996,#38997,#38998,#38999,#39000,#39001,#39002,#39003,#39004,#39005,#39006,
#39007,#39008,#39009,#39010,#39011,#39012,#39013,#39014,#39015,#39016,#39017,
#39018,#39019,#39020,#39021,#39022,#39023,#39024,#39025,#39026,#39027,#39028,
#39029,#39030,#39031,#39032,#39033,#39034,#39035,#39036,#39037,#39038,#39039,
#39040,#39041,#39042,#39043,#39044,#39045,#39046,#39047,#39048,#39049,#39050,
#39051,#39052,#39053,#39054,#39055,#39056,#39057,#39058,#39059,#39060,#39061,
#39062,#39063,#39064,#39065,#39066,#39067,#39068,#39069,#39070,#39071,#39072,
#39073,#39074,#39075,#39076,#39077,#39078,#39079,#39080,#39081,#39082,#39083,
#39084,#39085,#39086,#39087,#39088,#39089,#39090,#39091,#39092,#39093,#39094,
#39095,#39096,#39097,#39098,#39099,#39100,#39101,#39102,#39103,#39104,#39105,
#39106,#39107,#39108,#39109,#39110,#39111,#39112,#39113,#39114,#39115,#39116,
#39117,#39118,#39119,#39120),.UNSPECIFIED.,.F.,.F.,(4,3,3,3,3,3,3,3,3,3,
3,3,3,3,3,3,3,3,3,3,3,3,3,3,3,3,3,3,3,3,3,3,3,3,3,3,3,3,3,3,3,3,3,3,3,3,
3,3,3,3,3,3,3,3,3,3,3,3,3,3,3,3,3,3,3,3,3,3,3,3,3,3,3,3,3,3,4),(229.336263712056,
229.41886753326,229.501541636033,229.584074644522,229.66660240436,229.749143732478,
229.831922888221,229.914589512896,229.997424934172,230.080260355448,230.16400708815,
230.247650765166,230.331211509232,230.414709371189,230.498171871751,230.581617007243,
230.665062842086,230.748527437324,230.832080622746,230.915678456319,230.999410019181,
231.079243857647,231.162990590349,231.246634267365,231.330195011431,231.413692873388,
231.49715537395,231.580600509443,231.664046344285,231.747510939523,231.831064124945,
231.914661958518,231.99839352138,232.078227359846,232.161974092548,232.245617769564,
232.32917851363,232.412676375587,232.496138876149,232.579584011642,232.663029846485,
232.746494441723,232.830047627145,232.913645460718,232.99737702358,233.077210862045,
233.160957594747,233.244601271763,233.32816201583,233.411659877787,233.49512237835,
233.578567513842,233.662013348685,233.745477943923,233.829031129345,233.912628962918,
233.99636052578,234.076194364245,234.159941096947,234.243584773963,234.327145518029,
234.410643379986,234.494105880548,234.577551016041,234.660996850883,234.744461446121,
234.828014631543,234.911612465116,234.995344027978,235.075177866444,235.161656885001,
235.248006508427,235.334240268089,235.420341411725,235.506363821645,235.592303722112,
235.619449019236),.UNSPECIFIED.);
#380=B_SPLINE_CURVE_WITH_KNOTS('',3,(#39122,#39123,#39124,#39125,#39126,
#39127,#39128,#39129,#39130,#39131,#39132,#39133,#39134,#39135,#39136,#39137,
#39138,#39139,#39140,#39141,#39142,#39143,#39144,#39145,#39146,#39147,#39148,
#39149,#39150,#39151,#39152,#39153,#39154,#39155,#39156,#39157,#39158,#39159,
#39160,#39161,#39162,#39163,#39164,#39165,#39166,#39167,#39168,#39169,#39170,
#39171,#39172,#39173,#39174,#39175,#39176,#39177,#39178,#39179,#39180,#39181,
#39182,#39183,#39184,#39185,#39186,#39187,#39188,#39189,#39190,#39191,#39192,
#39193,#39194,#39195,#39196,#39197,#39198,#39199,#39200,#39201,#39202,#39203,
#39204,#39205,#39206,#39207,#39208,#39209,#39210,#39211,#39212,#39213,#39214,
#39215,#39216,#39217,#39218,#39219,#39220,#39221,#39222,#39223,#39224,#39225,
#39226,#39227,#39228,#39229,#39230,#39231,#39232,#39233,#39234,#39235,#39236,
#39237,#39238,#39239,#39240,#39241,#39242,#39243,#39244,#39245,#39246,#39247,
#39248,#39249,#39250,#39251,#39252,#39253,#39254,#39255,#39256,#39257,#39258,
#39259,#39260,#39261,#39262,#39263,#39264,#39265,#39266,#39267,#39268,#39269,
#39270,#39271,#39272,#39273,#39274,#39275,#39276,#39277,#39278,#39279,#39280,
#39281,#39282,#39283,#39284,#39285,#39286,#39287,#39288,#39289,#39290,#39291,
#39292,#39293,#39294,#39295,#39296,#39297,#39298,#39299,#39300,#39301,#39302,
#39303,#39304,#39305,#39306,#39307,#39308,#39309,#39310,#39311,#39312,#39313,
#39314,#39315,#39316,#39317,#39318,#39319,#39320,#39321,#39322,#39323,#39324,
#39325,#39326,#39327,#39328,#39329,#39330,#39331,#39332,#39333,#39334,#39335,
#39336,#39337,#39338,#39339,#39340,#39341,#39342,#39343,#39344,#39345,#39346,
#39347,#39348,#39349,#39350),.UNSPECIFIED.,.F.,.F.,(4,3,3,3,3,3,3,3,3,3,
3,3,3,3,3,3,3,3,3,3,3,3,3,3,3,3,3,3,3,3,3,3,3,3,3,3,3,3,3,3,3,3,3,3,3,3,
3,3,3,3,3,3,3,3,3,3,3,3,3,3,3,3,3,3,3,3,3,3,3,3,3,3,3,3,3,3,4),(223.053078404877,
223.087375840054,223.171122572756,223.254766249772,223.338326993838,223.421824855795,
223.505287356358,223.58873249185,223.672178326693,223.755642921931,223.839196107353,
223.922793940925,224.006525503787,224.086359342253,224.170106074955,224.253749751971,
224.337310496037,224.420808357994,224.504270858556,224.587715994049,224.671161828892,
224.75462642413,224.838179609551,224.921777443124,225.005509005986,225.085342844452,
225.169089577154,225.25273325417,225.336293998236,225.419791860193,225.503254360755,
225.586699496248,225.67014533109,225.753609926329,225.83716311175,225.920760945323,
226.004492508185,226.084326346651,226.168073079353,226.251716756369,226.335277500435,
226.418775362392,226.502237862955,226.585682998447,226.66912883329,226.752593428528,
226.836146613949,226.919744447522,227.003476010384,227.08330984885,227.167056581552,
227.250700258568,227.334261002635,227.417758864591,227.501221365154,227.584666500646,
227.668112335489,227.751576930728,227.835130116149,227.918727949722,228.002459512584,
228.08229335105,228.166040083752,228.249683760768,228.333244504835,228.416742366791,
228.500204867354,228.583650002846,228.667095837689,228.750560432927,228.834113618349,
228.917711451922,229.001443014784,229.081276853249,229.190064578712,229.296653912374,
229.336263711945),.UNSPECIFIED.);
#381=B_SPLINE_CURVE_WITH_KNOTS('',3,(#39352,#39353,#39354,#39355,#39356,
#39357,#39358,#39359,#39360,#39361,#39362,#39363,#39364,#39365,#39366,#39367,
#39368,#39369,#39370,#39371,#39372,#39373,#39374,#39375,#39376,#39377,#39378,
#39379,#39380,#39381,#39382,#39383,#39384,#39385,#39386,#39387,#39388,#39389,
#39390,#39391,#39392,#39393,#39394,#39395,#39396,#39397,#39398,#39399,#39400,
#39401,#39402,#39403,#39404,#39405,#39406,#39407,#39408,#39409,#39410,#39411,
#39412,#39413,#39414,#39415,#39416,#39417,#39418,#39419,#39420,#39421,#39422,
#39423,#39424,#39425,#39426,#39427,#39428,#39429,#39430,#39431,#39432,#39433,
#39434,#39435,#39436,#39437,#39438,#39439,#39440,#39441,#39442,#39443,#39444,
#39445,#39446,#39447,#39448,#39449,#39450,#39451,#39452,#39453,#39454,#39455,
#39456,#39457,#39458,#39459,#39460,#39461,#39462,#39463,#39464,#39465,#39466,
#39467,#39468,#39469,#39470,#39471,#39472,#39473,#39474,#39475,#39476,#39477,
#39478,#39479,#39480,#39481,#39482,#39483,#39484,#39485,#39486,#39487,#39488,
#39489,#39490,#39491,#39492,#39493,#39494,#39495,#39496,#39497,#39498,#39499,
#39500,#39501,#39502,#39503,#39504,#39505,#39506,#39507,#39508,#39509,#39510,
#39511,#39512,#39513,#39514,#39515,#39516,#39517,#39518,#39519,#39520,#39521,
#39522,#39523,#39524,#39525,#39526,#39527,#39528,#39529,#39530,#39531,#39532,
#39533,#39534,#39535,#39536,#39537,#39538,#39539,#39540,#39541,#39542,#39543,
#39544,#39545,#39546,#39547,#39548,#39549,#39550,#39551,#39552,#39553,#39554,
#39555,#39556,#39557,#39558,#39559,#39560,#39561,#39562,#39563,#39564,#39565,
#39566,#39567,#39568,#39569,#39570,#39571,#39572,#39573,#39574,#39575,#39576,
#39577,#39578,#39579,#39580),.UNSPECIFIED.,.F.,.F.,(4,3,3,3,3,3,3,3,3,3,
3,3,3,3,3,3,3,3,3,3,3,3,3,3,3,3,3,3,3,3,3,3,3,3,3,3,3,3,3,3,3,3,3,3,3,3,
3,3,3,3,3,3,3,3,3,3,3,3,3,3,3,3,3,3,3,3,3,3,3,3,3,3,3,3,3,3,4),(216.769893097874,
216.867988859855,216.966730771947,217.066196864284,217.093474826859,217.177221559561,
217.260865236577,217.344425980643,217.4279238426,217.511386343162,217.594831478654,
217.678277313497,217.761741908735,217.845295094157,217.928892927729,218.012624490591,
218.092458329058,218.17620506176,218.259848738776,218.343409482842,218.426907344799,
218.510369845361,218.593814980854,218.677260815696,218.760725410934,218.844278596356,
218.927876429929,219.011607992791,219.091441831257,219.175188563959,219.258832240975,
219.342392985041,219.425890846998,219.509353347561,219.592798483053,219.676244317896,
219.759708913134,219.843262098556,219.926859932128,220.01059149499,220.090425333456,
220.174172066158,220.257815743174,220.34137648724,220.424874349197,220.50833684976,
220.591781985252,220.675227820095,220.758692415333,220.842245600755,220.925843434327,
221.009574997189,221.089408835655,221.173155568357,221.256799245373,221.340359989439,
221.423857851396,221.507320351959,221.590765487451,221.674211322294,221.757675917532,
221.841229102954,221.924826936526,222.008558499388,222.088392337855,222.171674256109,
222.254853427668,222.337950444371,222.420985821213,222.503987612706,222.586973977605,
222.669963395455,222.7529743444,222.836072663398,222.919218957202,223.002488182695,
223.053078404729),.UNSPECIFIED.);
#382=B_SPLINE_CURVE_WITH_KNOTS('',3,(#39582,#39583,#39584,#39585,#39586,
#39587,#39588,#39589,#39590,#39591,#39592,#39593,#39594,#39595,#39596,#39597,
#39598,#39599,#39600,#39601,#39602,#39603,#39604,#39605,#39606,#39607,#39608,
#39609,#39610,#39611,#39612,#39613,#39614,#39615,#39616,#39617,#39618,#39619,
#39620,#39621,#39622,#39623,#39624,#39625,#39626,#39627,#39628,#39629,#39630,
#39631,#39632,#39633,#39634,#39635,#39636,#39637,#39638,#39639,#39640,#39641,
#39642,#39643,#39644,#39645,#39646,#39647,#39648,#39649,#39650,#39651,#39652,
#39653,#39654,#39655,#39656,#39657,#39658,#39659,#39660,#39661,#39662,#39663,
#39664,#39665,#39666,#39667,#39668,#39669,#39670,#39671,#39672,#39673,#39674,
#39675,#39676,#39677,#39678,#39679,#39680,#39681,#39682,#39683,#39684,#39685,
#39686,#39687,#39688,#39689,#39690,#39691,#39692,#39693,#39694,#39695,#39696,
#39697,#39698,#39699,#39700,#39701,#39702,#39703,#39704,#39705,#39706,#39707,
#39708,#39709,#39710,#39711,#39712,#39713,#39714,#39715,#39716,#39717,#39718,
#39719,#39720,#39721,#39722,#39723,#39724,#39725,#39726,#39727,#39728,#39729,
#39730,#39731,#39732,#39733,#39734,#39735,#39736,#39737,#39738,#39739,#39740,
#39741,#39742,#39743,#39744,#39745,#39746,#39747,#39748,#39749,#39750,#39751,
#39752,#39753,#39754,#39755,#39756,#39757,#39758,#39759,#39760,#39761,#39762,
#39763,#39764,#39765,#39766,#39767,#39768,#39769,#39770,#39771,#39772,#39773,
#39774,#39775,#39776,#39777,#39778,#39779,#39780,#39781,#39782,#39783,#39784,
#39785,#39786,#39787,#39788,#39789,#39790,#39791,#39792,#39793,#39794,#39795,
#39796,#39797,#39798,#39799,#39800,#39801,#39802,#39803,#39804,#39805,#39806,
#39807,#39808,#39809,#39810),.UNSPECIFIED.,.F.,.F.,(4,3,3,3,3,3,3,3,3,3,
3,3,3,3,3,3,3,3,3,3,3,3,3,3,3,3,3,3,3,3,3,3,3,3,3,3,3,3,3,3,3,3,3,3,3,3,
3,3,3,3,3,3,3,3,3,3,3,3,3,3,3,3,3,3,3,3,3,3,3,3,3,3,3,3,3,3,4),(210.486707790518,
210.570999537664,210.655305176302,210.739641535065,210.824025459423,210.908524456367,
210.993091242317,211.077790090279,211.099573813664,211.183320546366,211.266964223382,
211.350524967448,211.434022829405,211.517485329967,211.60093046546,211.684376300303,
211.767840895541,211.851394080962,211.934991914535,212.018723477397,212.098557315863,
212.182304048565,212.265947725581,212.349508469647,212.433006331604,212.516468832166,
212.599913967659,212.683359802502,212.76682439774,212.850377583162,212.933975416734,
213.017706979596,213.097540818062,213.181287550764,213.26493122778,213.348491971846,
213.431989833803,213.515452334366,213.598897469858,213.682343304701,213.765807899939,
213.849361085361,213.932958918933,214.016690481795,214.096524320261,214.180271052963,
214.263914729979,214.347475474046,214.430973336002,214.514435836565,214.597880972057,
214.6813268069,214.764791402138,214.84834458756,214.931942421133,215.015673983995,
215.09550782246,215.179254555162,215.262898232178,215.346458976244,215.4299568382,
215.513419338763,215.596864474255,215.680310309098,215.763774904336,215.847328089758,
215.930925923331,216.014657486193,216.09449132466,216.17891654629,216.262367135454,
216.345736920481,216.42904420361,216.514256427132,216.597501403593,216.683697250645,
216.769893097697),.UNSPECIFIED.);
#383=B_SPLINE_CURVE_WITH_KNOTS('',3,(#39812,#39813,#39814,#39815,#39816,
#39817,#39818,#39819,#39820,#39821,#39822,#39823,#39824,#39825,#39826,#39827,
#39828,#39829,#39830,#39831,#39832,#39833,#39834,#39835,#39836,#39837,#39838,
#39839,#39840,#39841,#39842,#39843,#39844,#39845,#39846,#39847,#39848,#39849,
#39850,#39851,#39852,#39853,#39854,#39855,#39856,#39857,#39858,#39859,#39860,
#39861,#39862,#39863,#39864,#39865,#39866,#39867,#39868,#39869,#39870,#39871,
#39872,#39873,#39874,#39875,#39876,#39877,#39878,#39879,#39880,#39881,#39882,
#39883,#39884,#39885,#39886,#39887,#39888,#39889,#39890,#39891,#39892,#39893,
#39894,#39895,#39896,#39897,#39898,#39899,#39900,#39901,#39902,#39903,#39904,
#39905,#39906,#39907,#39908,#39909,#39910,#39911,#39912,#39913,#39914,#39915,
#39916,#39917,#39918,#39919,#39920,#39921,#39922,#39923,#39924,#39925,#39926,
#39927,#39928,#39929,#39930,#39931,#39932,#39933,#39934,#39935,#39936,#39937,
#39938,#39939,#39940,#39941,#39942,#39943,#39944,#39945,#39946,#39947,#39948,
#39949,#39950,#39951,#39952,#39953,#39954,#39955,#39956,#39957,#39958,#39959,
#39960,#39961,#39962,#39963,#39964,#39965,#39966,#39967,#39968,#39969,#39970,
#39971,#39972,#39973,#39974,#39975,#39976,#39977,#39978,#39979,#39980,#39981,
#39982,#39983,#39984,#39985,#39986,#39987,#39988,#39989,#39990,#39991,#39992,
#39993,#39994,#39995,#39996,#39997,#39998,#39999,#40000,#40001,#40002,#40003,
#40004,#40005,#40006,#40007,#40008,#40009,#40010,#40011,#40012,#40013,#40014,
#40015,#40016,#40017,#40018,#40019,#40020,#40021,#40022,#40023,#40024,#40025,
#40026,#40027,#40028,#40029,#40030,#40031,#40032,#40033,#40034,#40035,#40036,
#40037,#40038,#40039,#40040),.UNSPECIFIED.,.F.,.F.,(4,3,3,3,3,3,3,3,3,3,
3,3,3,3,3,3,3,3,3,3,3,3,3,3,3,3,3,3,3,3,3,3,3,3,3,3,3,3,3,3,3,3,3,3,3,3,
3,3,3,3,3,3,3,3,3,3,3,3,3,3,3,3,3,3,3,3,3,3,3,3,3,3,3,3,3,3,4),(204.203522483473,
204.286193926472,204.368772304277,204.451278642249,204.533738282922,204.616173967715,
204.698604592558,204.781049046846,204.863576513138,204.946145767727,205.028845394083,
205.105672800469,205.189419533171,205.273063210187,205.356623954253,205.44012181621,
205.523584316772,205.607029452265,205.690475287107,205.773939882346,205.857493067767,
205.94109090134,206.024822464202,206.104656302668,206.18840303537,206.272046712386,
206.355607456452,206.439105318408,206.522567818971,206.606012954463,206.689458789306,
206.772923384544,206.856476569966,206.940074403538,207.0238059664,207.103639804867,
207.187386537569,207.271030214585,207.354590958651,207.438088820608,207.521551321171,
207.604996456663,207.688442291506,207.771906886744,207.855460072166,207.939057905738,
208.0227894686,208.102623307066,208.186370039768,208.270013716784,208.353574460851,
208.437072322808,208.52053482337,208.603979958862,208.687425793705,208.770890388943,
208.854443574365,208.938041407938,209.0217729708,209.101606809265,209.185353541967,
209.268997218983,209.35255796305,209.436055825006,209.519518325569,209.602963461062,
209.686409295904,209.769873891143,209.853427076564,209.937024910137,210.020756472999,
210.100590311465,210.197119681181,210.29081274856,210.388760269444,210.481685600267,
210.486707790327),.UNSPECIFIED.);
#384=B_SPLINE_CURVE_WITH_KNOTS('',3,(#40042,#40043,#40044,#40045,#40046,
#40047,#40048,#40049,#40050,#40051,#40052,#40053,#40054,#40055,#40056,#40057,
#40058,#40059,#40060,#40061,#40062,#40063,#40064,#40065,#40066,#40067,#40068,
#40069,#40070,#40071,#40072,#40073,#40074,#40075,#40076,#40077,#40078,#40079,
#40080,#40081,#40082,#40083,#40084,#40085,#40086,#40087,#40088,#40089,#40090,
#40091,#40092,#40093,#40094,#40095,#40096,#40097,#40098,#40099,#40100,#40101,
#40102,#40103,#40104,#40105,#40106,#40107,#40108,#40109,#40110,#40111,#40112,
#40113,#40114,#40115,#40116,#40117,#40118,#40119,#40120,#40121,#40122,#40123,
#40124,#40125,#40126,#40127,#40128,#40129,#40130,#40131,#40132,#40133,#40134,
#40135,#40136,#40137,#40138,#40139,#40140,#40141,#40142,#40143,#40144,#40145,
#40146,#40147,#40148,#40149,#40150,#40151,#40152,#40153,#40154,#40155,#40156,
#40157,#40158,#40159,#40160,#40161,#40162,#40163,#40164,#40165,#40166,#40167,
#40168,#40169,#40170,#40171,#40172,#40173,#40174,#40175,#40176,#40177,#40178,
#40179,#40180,#40181,#40182,#40183,#40184,#40185,#40186,#40187,#40188,#40189,
#40190,#40191,#40192,#40193,#40194,#40195,#40196,#40197,#40198,#40199,#40200,
#40201,#40202,#40203,#40204,#40205,#40206,#40207,#40208,#40209,#40210,#40211,
#40212,#40213,#40214,#40215,#40216,#40217,#40218,#40219,#40220,#40221,#40222,
#40223,#40224,#40225,#40226,#40227,#40228,#40229,#40230,#40231,#40232,#40233,
#40234,#40235,#40236,#40237,#40238,#40239,#40240,#40241,#40242,#40243,#40244,
#40245,#40246,#40247,#40248,#40249,#40250,#40251,#40252,#40253,#40254,#40255,
#40256,#40257,#40258,#40259,#40260,#40261,#40262,#40263,#40264,#40265,#40266,
#40267),.UNSPECIFIED.,.F.,.F.,(4,3,3,3,3,3,3,3,3,3,3,3,3,3,3,3,3,3,3,3,
3,3,3,3,3,3,3,3,3,3,3,3,3,3,3,3,3,3,3,3,3,3,3,3,3,3,3,3,3,3,3,3,3,3,3,3,
3,3,3,3,3,3,3,3,3,3,3,3,3,3,3,3,3,3,3,4),(197.920337176159,198.042804749541,
198.112788285075,198.196535017777,198.280178694793,198.363739438859,198.447237300816,
198.530699801378,198.614144936871,198.697590771713,198.781055366951,198.864608552373,
198.948206385946,199.031937948808,199.111771787274,199.195518519976,199.279162196992,
199.362722941058,199.446220803015,199.529683303578,199.61312843907,199.696574273913,
199.780038869151,199.863592054573,199.947189888145,200.030921451007,200.110755289473,
200.194502022175,200.278145699191,200.361706443257,200.445204305214,200.528666805777,
200.612111941269,200.695557776112,200.77902237135,200.862575556772,200.946173390344,
201.029904953206,201.109738791672,201.193485524374,201.27712920139,201.360689945456,
201.444187807413,201.527650307975,201.611095443468,201.694541278311,201.778005873549,
201.86155905897,201.945156892543,202.028888455405,202.108722293871,202.192469026573,
202.276112703589,202.359673447655,202.443171309612,202.526633810175,202.610078945667,
202.69352478051,202.776989375748,202.86054256117,202.944140394743,203.027871957605,
203.10770579607,203.191452528772,203.275096205788,203.358656949854,203.442154811811,
203.525617312373,203.609062447865,203.692508282708,203.775972877946,203.859526063368,
203.94312389694,204.026855459802,204.10668929827,204.203522483338),
 .UNSPECIFIED.);
#385=B_SPLINE_CURVE_WITH_KNOTS('',3,(#40269,#40270,#40271,#40272,#40273,
#40274,#40275,#40276,#40277,#40278,#40279,#40280,#40281,#40282,#40283,#40284,
#40285,#40286,#40287,#40288,#40289,#40290,#40291,#40292,#40293,#40294,#40295,
#40296,#40297,#40298,#40299,#40300,#40301,#40302,#40303,#40304,#40305,#40306,
#40307,#40308,#40309,#40310,#40311,#40312,#40313,#40314,#40315,#40316,#40317,
#40318,#40319,#40320,#40321,#40322,#40323,#40324,#40325,#40326,#40327,#40328,
#40329,#40330,#40331,#40332,#40333,#40334,#40335,#40336,#40337,#40338,#40339,
#40340,#40341,#40342,#40343,#40344,#40345,#40346,#40347,#40348,#40349,#40350,
#40351,#40352,#40353,#40354,#40355,#40356,#40357,#40358,#40359,#40360,#40361,
#40362,#40363,#40364,#40365,#40366,#40367,#40368,#40369,#40370,#40371,#40372,
#40373,#40374,#40375,#40376,#40377,#40378,#40379,#40380,#40381,#40382,#40383,
#40384,#40385,#40386,#40387,#40388,#40389,#40390,#40391,#40392,#40393,#40394,
#40395,#40396,#40397,#40398,#40399,#40400,#40401,#40402,#40403,#40404,#40405,
#40406,#40407,#40408,#40409,#40410,#40411,#40412,#40413,#40414,#40415,#40416,
#40417,#40418,#40419,#40420,#40421,#40422,#40423,#40424,#40425,#40426,#40427,
#40428,#40429,#40430,#40431,#40432,#40433,#40434,#40435,#40436,#40437,#40438,
#40439,#40440,#40441,#40442,#40443,#40444,#40445,#40446,#40447,#40448,#40449,
#40450,#40451,#40452,#40453,#40454,#40455,#40456,#40457,#40458,#40459,#40460,
#40461,#40462,#40463,#40464,#40465,#40466,#40467,#40468,#40469,#40470,#40471,
#40472,#40473,#40474,#40475,#40476,#40477,#40478,#40479,#40480,#40481,#40482,
#40483,#40484,#40485,#40486,#40487,#40488,#40489,#40490,#40491,#40492,#40493,
#40494,#40495,#40496,#40497),.UNSPECIFIED.,.F.,.F.,(4,3,3,3,3,3,3,3,3,3,
3,3,3,3,3,3,3,3,3,3,3,3,3,3,3,3,3,3,3,3,3,3,3,3,3,3,3,3,3,3,3,3,3,3,3,3,
3,3,3,3,3,3,3,3,3,3,3,3,3,3,3,3,3,3,3,3,3,3,3,3,3,3,3,3,3,3,4),(191.637151869127,
191.72523147956,191.813451550297,191.901902961679,191.9904796452,192.079262046608,
192.11888727188,192.202634004582,192.286277681598,192.369838425664,192.453336287621,
192.536798788184,192.620243923676,192.703689758519,192.787154353757,192.870707539179,
192.954305372751,193.038036935613,193.117870774079,193.201617506781,193.285261183797,
193.368821927863,193.45231978982,193.535782290382,193.619227425875,193.702673260717,
193.786137855955,193.869691041377,193.95328887495,194.037020437812,194.116854276278,
194.20060100898,194.284244685996,194.367805430062,194.451303292019,194.534765792582,
194.618210928074,194.701656762917,194.785121358155,194.868674543577,194.952272377149,
195.036003940011,195.115837778477,195.199584511179,195.283228188195,195.366788932261,
195.450286794218,195.53374929478,195.617194430272,195.700640265115,195.784104860353,
195.867658045775,195.951255879348,196.034987442209,196.114821280676,196.198568013378,
196.282211690394,196.36577243446,196.449270296417,196.53273279698,196.616177932472,
196.699623767315,196.783088362553,196.866641547975,196.950239381547,197.033970944409,
197.113804782875,197.196328092342,197.278748420473,197.361075187093,197.443349557154,
197.525590589424,197.607817311615,197.690081386651,197.772363362024,197.854731017392,
197.920337176039),.UNSPECIFIED.);
#386=B_SPLINE_CURVE_WITH_KNOTS('',3,(#40499,#40500,#40501,#40502,#40503,
#40504,#40505,#40506,#40507,#40508,#40509,#40510,#40511,#40512,#40513,#40514,
#40515,#40516,#40517,#40518,#40519,#40520,#40521,#40522,#40523,#40524,#40525,
#40526,#40527,#40528,#40529,#40530,#40531,#40532,#40533,#40534,#40535,#40536,
#40537,#40538,#40539,#40540,#40541,#40542,#40543,#40544,#40545,#40546,#40547,
#40548,#40549,#40550,#40551,#40552,#40553,#40554,#40555,#40556,#40557,#40558,
#40559,#40560,#40561,#40562,#40563,#40564,#40565,#40566,#40567,#40568,#40569,
#40570,#40571,#40572,#40573,#40574,#40575,#40576,#40577,#40578,#40579,#40580,
#40581,#40582,#40583,#40584,#40585,#40586,#40587,#40588,#40589,#40590,#40591,
#40592,#40593,#40594,#40595,#40596,#40597,#40598,#40599,#40600,#40601,#40602,
#40603,#40604,#40605,#40606,#40607,#40608,#40609,#40610,#40611,#40612,#40613,
#40614,#40615,#40616,#40617,#40618,#40619,#40620,#40621,#40622,#40623,#40624,
#40625,#40626,#40627,#40628,#40629,#40630,#40631,#40632,#40633,#40634,#40635,
#40636,#40637,#40638,#40639,#40640,#40641,#40642,#40643,#40644,#40645,#40646,
#40647,#40648,#40649,#40650,#40651,#40652,#40653,#40654,#40655,#40656,#40657,
#40658,#40659,#40660,#40661,#40662,#40663,#40664,#40665,#40666,#40667,#40668,
#40669,#40670,#40671,#40672,#40673,#40674,#40675,#40676,#40677,#40678,#40679,
#40680,#40681,#40682,#40683,#40684,#40685,#40686,#40687,#40688,#40689,#40690,
#40691,#40692,#40693,#40694,#40695,#40696,#40697,#40698,#40699,#40700,#40701,
#40702,#40703,#40704,#40705,#40706,#40707,#40708,#40709,#40710,#40711,#40712,
#40713,#40714,#40715,#40716,#40717,#40718,#40719,#40720,#40721,#40722,#40723,
#40724,#40725,#40726,#40727),.UNSPECIFIED.,.F.,.F.,(4,3,3,3,3,3,3,3,3,3,
3,3,3,3,3,3,3,3,3,3,3,3,3,3,3,3,3,3,3,3,3,3,3,3,3,3,3,3,3,3,3,3,3,3,3,3,
3,3,3,3,3,3,3,3,3,3,3,3,3,3,3,3,3,3,3,3,3,3,3,3,3,3,3,3,3,3,4),(185.353966561907,
185.436430980761,185.522500390501,185.604872317226,185.687231798795,185.769597769302,
185.851989165541,185.934469289462,186.017001705857,186.099650436777,186.124986258685,
186.208732991387,186.292376668403,186.375937412469,186.459435274426,186.542897774989,
186.626342910481,186.709788745324,186.793253340562,186.876806525984,186.960404359557,
187.044135922419,187.123969760884,187.207716493586,187.291360170601,187.374920914668,
187.458418776624,187.541881277187,187.625326412679,187.708772247522,187.79223684276,
187.875790028182,187.959387861754,188.043119424616,188.122953263083,188.206699995785,
188.290343672801,188.373904416867,188.457402278824,188.540864779386,188.624309914879,
188.707755749722,188.79122034496,188.874773530382,188.958371363954,189.042102926816,
189.121936765282,189.205683497984,189.289327175,189.372887919066,189.456385781023,
189.539848281586,189.623293417078,189.706739251921,189.790203847159,189.873757032581,
189.957354866153,190.041086429015,190.120920267481,190.204667000183,190.288310677198,
190.371871421265,190.455369283222,190.538831783784,190.622276919276,190.70572275412,
190.789187349358,190.87274053478,190.956338368352,191.040069931214,191.11990376968,
191.207292110406,191.294538799997,191.381603868696,191.468562696466,191.555387492085,
191.637151868979),.UNSPECIFIED.);
#387=B_SPLINE_CURVE_WITH_KNOTS('',3,(#40729,#40730,#40731,#40732,#40733,
#40734,#40735,#40736,#40737,#40738,#40739,#40740,#40741,#40742,#40743,#40744,
#40745,#40746,#40747,#40748,#40749,#40750,#40751,#40752,#40753,#40754,#40755,
#40756,#40757,#40758,#40759,#40760,#40761,#40762,#40763,#40764,#40765,#40766,
#40767,#40768,#40769,#40770,#40771,#40772,#40773,#40774,#40775,#40776,#40777,
#40778,#40779,#40780,#40781,#40782,#40783,#40784,#40785,#40786,#40787,#40788,
#40789,#40790,#40791,#40792,#40793,#40794,#40795,#40796,#40797,#40798,#40799,
#40800,#40801,#40802,#40803,#40804,#40805,#40806,#40807,#40808,#40809,#40810,
#40811,#40812,#40813,#40814,#40815,#40816,#40817,#40818,#40819,#40820,#40821,
#40822,#40823,#40824,#40825,#40826,#40827,#40828,#40829,#40830,#40831,#40832,
#40833,#40834,#40835,#40836,#40837,#40838,#40839,#40840,#40841,#40842,#40843,
#40844,#40845,#40846,#40847,#40848,#40849,#40850,#40851,#40852,#40853,#40854,
#40855,#40856,#40857,#40858,#40859,#40860,#40861,#40862,#40863,#40864,#40865,
#40866,#40867,#40868,#40869,#40870,#40871,#40872,#40873,#40874,#40875,#40876,
#40877,#40878,#40879,#40880,#40881,#40882,#40883,#40884,#40885,#40886,#40887,
#40888,#40889,#40890,#40891,#40892,#40893,#40894,#40895,#40896,#40897,#40898,
#40899,#40900,#40901,#40902,#40903,#40904,#40905,#40906,#40907,#40908,#40909,
#40910,#40911,#40912,#40913,#40914,#40915,#40916,#40917,#40918,#40919,#40920,
#40921,#40922,#40923,#40924,#40925,#40926,#40927,#40928,#40929,#40930,#40931,
#40932,#40933,#40934,#40935,#40936,#40937,#40938,#40939,#40940,#40941,#40942,
#40943,#40944,#40945,#40946,#40947,#40948,#40949,#40950,#40951,#40952,#40953,
#40954),.UNSPECIFIED.,.F.,.F.,(4,3,3,3,3,3,3,3,3,3,3,3,3,3,3,3,3,3,3,3,
3,3,3,3,3,3,3,3,3,3,3,3,3,3,3,3,3,3,3,3,3,3,3,3,3,3,3,3,3,3,3,3,3,3,3,3,
3,3,3,3,3,3,3,3,3,3,3,3,3,3,3,3,3,3,3,4),(179.07078125462,179.13210174329,
179.215848475992,179.299492153008,179.383052897074,179.466550759031,179.550013259594,
179.633458395086,179.716904229929,179.800368825167,179.883922010589,179.967519844162,
180.051251407024,180.13108524549,180.214831978192,180.298475655208,180.382036399274,
180.465534261231,180.548996761794,180.632441897286,180.715887732129,180.799352327367,
180.882905512789,180.966503346362,181.050234909224,181.130068747689,181.213815480391,
181.297459157407,181.381019901473,181.46451776343,181.547980263992,181.631425399484,
181.714871234327,181.798335829565,181.881889014987,181.96548684856,182.049218411421,
182.129052249888,182.21279898259,182.296442659606,182.380003403672,182.463501265629,
182.546963766192,182.630408901684,182.713854736527,182.797319331765,182.880872517187,
182.964470350759,183.048201913621,183.128035752087,183.211782484789,183.295426161805,
183.378986905871,183.462484767828,183.545947268391,183.629392403883,183.712838238726,
183.796302833964,183.879856019385,183.963453852958,184.04718541582,184.127019254286,
184.210765986988,184.294409664004,184.37797040807,184.461468270027,184.544930770589,
184.628375906081,184.711821740924,184.795286336162,184.878839521584,184.962437355157,
185.046168918018,185.126002756485,185.239984659142,185.353966561799),
 .UNSPECIFIED.);
#388=B_SPLINE_CURVE_WITH_KNOTS('',3,(#40956,#40957,#40958,#40959,#40960,
#40961,#40962,#40963,#40964,#40965,#40966,#40967,#40968,#40969,#40970,#40971,
#40972,#40973,#40974,#40975,#40976,#40977,#40978,#40979,#40980,#40981,#40982,
#40983,#40984,#40985,#40986,#40987,#40988,#40989,#40990,#40991,#40992,#40993,
#40994,#40995,#40996,#40997,#40998,#40999,#41000,#41001,#41002,#41003,#41004,
#41005,#41006,#41007,#41008,#41009,#41010,#41011,#41012,#41013,#41014,#41015,
#41016,#41017,#41018,#41019,#41020,#41021,#41022,#41023,#41024,#41025,#41026,
#41027,#41028,#41029,#41030,#41031,#41032,#41033,#41034,#41035,#41036,#41037,
#41038,#41039,#41040,#41041,#41042,#41043,#41044,#41045,#41046,#41047,#41048,
#41049,#41050,#41051,#41052,#41053,#41054,#41055,#41056,#41057,#41058,#41059,
#41060,#41061,#41062,#41063,#41064,#41065,#41066,#41067,#41068,#41069,#41070,
#41071,#41072,#41073,#41074,#41075,#41076,#41077,#41078,#41079,#41080,#41081,
#41082,#41083,#41084,#41085,#41086,#41087,#41088,#41089,#41090,#41091,#41092,
#41093,#41094,#41095,#41096,#41097,#41098,#41099,#41100,#41101,#41102,#41103,
#41104,#41105,#41106,#41107,#41108,#41109,#41110,#41111,#41112,#41113,#41114,
#41115,#41116,#41117,#41118,#41119,#41120,#41121,#41122,#41123,#41124,#41125,
#41126,#41127,#41128,#41129,#41130,#41131,#41132,#41133,#41134,#41135,#41136,
#41137,#41138,#41139,#41140,#41141,#41142,#41143,#41144,#41145,#41146,#41147,
#41148,#41149,#41150,#41151,#41152,#41153,#41154,#41155,#41156,#41157,#41158,
#41159,#41160,#41161,#41162,#41163,#41164,#41165,#41166,#41167,#41168,#41169,
#41170,#41171,#41172,#41173,#41174,#41175,#41176,#41177,#41178,#41179,#41180,
#41181,#41182,#41183,#41184),.UNSPECIFIED.,.F.,.F.,(4,3,3,3,3,3,3,3,3,3,
3,3,3,3,3,3,3,3,3,3,3,3,3,3,3,3,3,3,3,3,3,3,3,3,3,3,3,3,3,3,3,3,3,3,3,3,
3,3,3,3,3,3,3,3,3,3,3,3,3,3,3,3,3,3,3,3,3,3,3,3,3,3,3,3,3,3,4),(172.787595947634,
172.883336957541,172.979547986538,173.076358533046,173.138200730095,173.221947462797,
173.305591139813,173.389151883879,173.472649745836,173.556112246399,173.639557381891,
173.723003216734,173.806467811972,173.890020997394,173.973618830966,174.057350393828,
174.137184232295,174.220930964997,174.304574642013,174.388135386079,174.471633248036,
174.555095748599,174.638540884091,174.721986718934,174.805451314172,174.889004499594,
174.972602333167,175.056333896029,175.136167734494,175.219914467196,175.303558144212,
175.387118888278,175.470616750235,175.554079250797,175.637524386289,175.720970221132,
175.80443481637,175.887988001792,175.971585835364,176.055317398226,176.135151236693,
176.218897969395,176.302541646411,176.386102390477,176.469600252434,176.553062752997,
176.636507888489,176.719953723332,176.80341831857,176.886971503992,176.970569337564,
177.054300900426,177.134134738892,177.217881471594,177.30152514861,177.385085892676,
177.468583754633,177.552046255196,177.635491390688,177.718937225531,177.802401820769,
177.885955006191,177.969552839763,178.053284402625,178.133118241091,178.216112772867,
178.299004813803,178.381815209239,178.467935964897,178.550651613485,178.633353651688,
178.716060779604,178.79879169783,178.881607801925,178.964474423694,179.047453126179,
179.070781254507),.UNSPECIFIED.);
#389=B_SPLINE_CURVE_WITH_KNOTS('',3,(#41186,#41187,#41188,#41189,#41190,
#41191,#41192,#41193,#41194,#41195,#41196,#41197,#41198,#41199,#41200,#41201,
#41202,#41203,#41204,#41205,#41206,#41207,#41208,#41209,#41210,#41211,#41212,
#41213,#41214,#41215,#41216,#41217,#41218,#41219,#41220,#41221,#41222,#41223,
#41224,#41225,#41226,#41227,#41228,#41229,#41230,#41231,#41232,#41233,#41234,
#41235,#41236,#41237,#41238,#41239,#41240,#41241,#41242,#41243,#41244,#41245,
#41246,#41247,#41248,#41249,#41250,#41251,#41252,#41253,#41254,#41255,#41256,
#41257,#41258,#41259,#41260,#41261,#41262,#41263,#41264,#41265,#41266,#41267,
#41268,#41269,#41270,#41271,#41272,#41273,#41274,#41275,#41276,#41277,#41278,
#41279,#41280,#41281,#41282,#41283,#41284,#41285,#41286,#41287,#41288,#41289,
#41290,#41291,#41292,#41293,#41294,#41295,#41296,#41297,#41298,#41299,#41300,
#41301,#41302,#41303,#41304,#41305,#41306,#41307,#41308,#41309,#41310,#41311,
#41312,#41313,#41314,#41315,#41316,#41317,#41318,#41319,#41320,#41321,#41322,
#41323,#41324,#41325,#41326,#41327,#41328,#41329,#41330,#41331,#41332,#41333,
#41334,#41335,#41336,#41337,#41338,#41339,#41340,#41341,#41342,#41343,#41344,
#41345,#41346,#41347,#41348,#41349,#41350,#41351,#41352,#41353,#41354,#41355,
#41356,#41357,#41358,#41359,#41360,#41361,#41362,#41363,#41364,#41365,#41366,
#41367,#41368,#41369,#41370,#41371,#41372,#41373,#41374,#41375,#41376,#41377,
#41378,#41379,#41380,#41381,#41382,#41383,#41384,#41385,#41386,#41387,#41388,
#41389,#41390,#41391,#41392,#41393,#41394,#41395,#41396,#41397,#41398,#41399,
#41400,#41401,#41402,#41403,#41404,#41405,#41406,#41407,#41408,#41409,#41410,
#41411,#41412,#41413,#41414),.UNSPECIFIED.,.F.,.F.,(4,3,3,3,3,3,3,3,3,3,
3,3,3,3,3,3,3,3,3,3,3,3,3,3,3,3,3,3,3,3,3,3,3,3,3,3,3,3,3,3,3,3,3,3,3,3,
3,3,3,3,3,3,3,3,3,3,3,3,3,3,3,3,3,3,3,3,3,3,3,3,3,3,3,3,3,3,4),(166.504410640261,
166.588207254555,166.672002919908,166.755815193113,166.839661637873,166.923612475455,
167.007620588218,167.091764594634,167.1442997169,167.228046449602,167.311690126618,
167.395250870684,167.478748732641,167.562211233204,167.645656368696,167.729102203539,
167.812566798777,167.896119984199,167.979717817772,168.063449380634,168.1432832191,
168.227029951802,168.310673628818,168.394234372884,168.477732234841,168.561194735404,
168.644639870896,168.728085705739,168.811550300977,168.895103486399,168.978701319971,
169.062432882833,169.142266721299,169.226013454001,169.309657131016,169.393217875083,
169.47671573704,169.560178237602,169.643623373095,169.727069207937,169.810533803176,
169.894086988598,169.97768482217,170.061416385032,170.141250223498,170.2249969562,
170.308640633216,170.392201377282,170.475699239238,170.559161739801,170.642606875293,
170.726052710136,170.809517305374,170.893070490796,170.976668324368,171.06039988723,
171.140233725697,171.223980458399,171.307624135415,171.391184879481,171.474682741438,
171.558145242,171.641590377492,171.725036212335,171.808500807573,171.892053992995,
171.975651826568,172.05938338943,172.139217227896,172.223198945279,172.307077676614,
172.390871343758,172.474597806455,172.558275915806,172.641924630996,172.725578355938,
172.78759594744),.UNSPECIFIED.);
#390=B_SPLINE_CURVE_WITH_KNOTS('',3,(#41416,#41417,#41418,#41419,#41420,
#41421,#41422,#41423,#41424,#41425,#41426,#41427,#41428,#41429,#41430,#41431,
#41432,#41433,#41434,#41435,#41436,#41437,#41438,#41439,#41440,#41441,#41442,
#41443,#41444,#41445,#41446,#41447,#41448,#41449,#41450,#41451,#41452,#41453,
#41454,#41455,#41456,#41457,#41458,#41459,#41460,#41461,#41462,#41463,#41464,
#41465,#41466,#41467,#41468,#41469,#41470,#41471,#41472,#41473,#41474,#41475,
#41476,#41477,#41478,#41479,#41480,#41481,#41482,#41483,#41484,#41485,#41486,
#41487,#41488,#41489,#41490,#41491,#41492,#41493,#41494,#41495,#41496,#41497,
#41498,#41499,#41500,#41501,#41502,#41503,#41504,#41505,#41506,#41507,#41508,
#41509,#41510,#41511,#41512,#41513,#41514,#41515,#41516,#41517,#41518,#41519,
#41520,#41521,#41522,#41523,#41524,#41525,#41526,#41527,#41528,#41529,#41530,
#41531,#41532,#41533,#41534,#41535,#41536,#41537,#41538,#41539,#41540,#41541,
#41542,#41543,#41544,#41545,#41546,#41547,#41548,#41549,#41550,#41551,#41552,
#41553,#41554,#41555,#41556,#41557,#41558,#41559,#41560,#41561,#41562,#41563,
#41564,#41565,#41566,#41567,#41568,#41569,#41570,#41571,#41572,#41573,#41574,
#41575,#41576,#41577,#41578,#41579,#41580,#41581,#41582,#41583,#41584,#41585,
#41586,#41587,#41588,#41589,#41590,#41591,#41592,#41593,#41594,#41595,#41596,
#41597,#41598,#41599,#41600,#41601,#41602,#41603,#41604,#41605,#41606,#41607,
#41608,#41609,#41610,#41611,#41612,#41613,#41614,#41615,#41616,#41617,#41618,
#41619,#41620,#41621,#41622,#41623,#41624,#41625,#41626,#41627,#41628,#41629,
#41630,#41631,#41632,#41633,#41634,#41635,#41636,#41637,#41638,#41639,#41640,
#41641,#41642,#41643,#41644),.UNSPECIFIED.,.F.,.F.,(4,3,3,3,3,3,3,3,3,3,
3,3,3,3,3,3,3,3,3,3,3,3,3,3,3,3,3,3,3,3,3,3,3,3,3,3,3,3,3,3,3,3,3,3,3,3,
3,3,3,3,3,3,3,3,3,3,3,3,3,3,3,3,3,3,3,3,3,3,3,3,3,3,3,3,3,3,4),(160.221225333203,
160.304117287473,160.386911848399,160.469629902408,160.554726002571,160.637362369371,
160.719989807647,160.802627071407,160.889569979481,160.972329090611,161.055143868158,
161.138072213799,161.150398703705,161.234145436407,161.317789113423,161.401349857489,
161.484847719446,161.568310220008,161.6517553555,161.735201190343,161.818665785581,
161.902218971003,161.985816804576,162.069548367437,162.149382205905,162.233128938607,
162.316772615623,162.400333359689,162.483831221646,162.567293722209,162.650738857701,
162.734184692544,162.817649287782,162.901202473204,162.984800306776,163.068531869638,
163.148365708104,163.232112440806,163.315756117821,163.399316861888,163.482814723845,
163.566277224407,163.6497223599,163.733168194743,163.816632789981,163.900185975403,
163.983783808975,164.067515371837,164.147349210303,164.231095943005,164.314739620021,
164.398300364087,164.481798226044,164.565260726606,164.648705862099,164.732151696941,
164.815616292179,164.899169477601,164.982767311174,165.066498874036,165.146332712502,
165.230079445204,165.31372312222,165.397283866286,165.480781728243,165.564244228806,
165.647689364298,165.731135199141,165.81459979438,165.898152979801,165.981750813374,
166.065482376236,166.145316214701,166.24136187852,166.337061354585,166.432099443715,
166.504410640063),.UNSPECIFIED.);
#391=B_SPLINE_CURVE_WITH_KNOTS('',3,(#41646,#41647,#41648,#41649,#41650,
#41651,#41652,#41653,#41654,#41655,#41656,#41657,#41658,#41659,#41660,#41661,
#41662,#41663,#41664,#41665,#41666,#41667,#41668,#41669,#41670,#41671,#41672,
#41673,#41674,#41675,#41676,#41677,#41678,#41679,#41680,#41681,#41682,#41683,
#41684,#41685,#41686,#41687,#41688,#41689,#41690,#41691,#41692,#41693,#41694,
#41695,#41696,#41697,#41698,#41699,#41700,#41701,#41702,#41703,#41704,#41705,
#41706,#41707,#41708,#41709,#41710,#41711,#41712,#41713,#41714,#41715,#41716,
#41717,#41718,#41719,#41720,#41721,#41722,#41723,#41724,#41725,#41726,#41727,
#41728,#41729,#41730,#41731,#41732,#41733,#41734,#41735,#41736,#41737,#41738,
#41739,#41740,#41741,#41742,#41743,#41744,#41745,#41746,#41747,#41748,#41749,
#41750,#41751,#41752,#41753,#41754,#41755,#41756,#41757,#41758,#41759,#41760,
#41761,#41762,#41763,#41764,#41765,#41766,#41767,#41768,#41769,#41770,#41771,
#41772,#41773,#41774,#41775,#41776,#41777,#41778,#41779,#41780,#41781,#41782,
#41783,#41784,#41785,#41786,#41787,#41788,#41789,#41790,#41791,#41792,#41793,
#41794,#41795,#41796,#41797,#41798,#41799,#41800,#41801,#41802,#41803,#41804,
#41805,#41806,#41807,#41808,#41809,#41810,#41811,#41812,#41813,#41814,#41815,
#41816,#41817,#41818,#41819,#41820,#41821,#41822,#41823,#41824,#41825,#41826,
#41827,#41828,#41829,#41830,#41831,#41832,#41833,#41834,#41835,#41836,#41837,
#41838,#41839,#41840,#41841,#41842,#41843,#41844,#41845,#41846,#41847,#41848,
#41849,#41850,#41851,#41852,#41853,#41854,#41855,#41856,#41857,#41858,#41859,
#41860,#41861,#41862,#41863,#41864,#41865,#41866,#41867,#41868,#41869,#41870,
#41871),.UNSPECIFIED.,.F.,.F.,(4,3,3,3,3,3,3,3,3,3,3,3,3,3,3,3,3,3,3,3,
3,3,3,3,3,3,3,3,3,3,3,3,3,3,3,3,3,3,3,3,3,3,3,3,3,3,3,3,3,3,3,3,3,3,3,3,
3,3,3,3,3,3,3,3,3,3,3,3,3,3,3,3,3,3,3,4),(153.938040025902,154.052832737468,
154.157514188311,154.241260921013,154.324904598029,154.408465342096,154.491963204053,
154.575425704616,154.658870840108,154.742316674951,154.82578127019,154.909334455612,
154.992932289184,155.076663852047,155.15649769051,155.240244423212,155.323888100228,
155.407448844294,155.490946706251,155.574409206814,155.657854342306,155.741300177149,
155.824764772387,155.908317957809,155.991915791382,156.075647354244,156.15548119271,
156.239227925412,156.322871602428,156.406432346494,156.489930208451,156.573392709014,
156.656837844506,156.740283679349,156.823748274587,156.907301460009,156.990899293581,
157.074630856443,157.154464694909,157.238211427611,157.321855104627,157.405415848693,
157.48891371065,157.572376211213,157.655821346705,157.739267181548,157.822731776786,
157.906284962208,157.98988279578,158.073614358642,158.153448197108,158.23719492981,
158.320838606826,158.404399350892,158.487897212849,158.571359713412,158.654804848904,
158.738250683747,158.821715278985,158.905268464407,158.988866297979,159.072597860841,
159.152431699307,159.236178432009,159.319822109024,159.403382853091,159.486880715047,
159.57034321561,159.653788351102,159.737234185945,159.820698781183,159.904251966605,
159.987849800177,160.071581363039,160.151415201506,160.221225333081),
 .UNSPECIFIED.);
#392=B_SPLINE_CURVE_WITH_KNOTS('',3,(#41873,#41874,#41875,#41876,#41877,
#41878,#41879,#41880,#41881,#41882,#41883,#41884,#41885,#41886,#41887,#41888,
#41889,#41890,#41891,#41892,#41893,#41894,#41895,#41896,#41897,#41898,#41899,
#41900,#41901,#41902,#41903,#41904,#41905,#41906,#41907,#41908,#41909,#41910,
#41911,#41912,#41913,#41914,#41915,#41916,#41917,#41918,#41919,#41920,#41921,
#41922,#41923,#41924,#41925,#41926,#41927,#41928,#41929,#41930,#41931,#41932,
#41933,#41934,#41935,#41936,#41937,#41938,#41939,#41940,#41941,#41942,#41943,
#41944,#41945,#41946,#41947,#41948,#41949,#41950,#41951,#41952,#41953,#41954,
#41955,#41956,#41957,#41958,#41959,#41960,#41961,#41962,#41963,#41964,#41965,
#41966,#41967,#41968,#41969,#41970,#41971,#41972,#41973,#41974,#41975,#41976,
#41977,#41978,#41979,#41980,#41981,#41982,#41983,#41984,#41985,#41986,#41987,
#41988,#41989,#41990,#41991,#41992,#41993,#41994,#41995,#41996,#41997,#41998,
#41999,#42000,#42001,#42002,#42003,#42004,#42005,#42006,#42007,#42008,#42009,
#42010,#42011,#42012,#42013,#42014,#42015,#42016,#42017,#42018,#42019,#42020,
#42021,#42022,#42023,#42024,#42025,#42026,#42027,#42028,#42029,#42030,#42031,
#42032,#42033,#42034,#42035,#42036,#42037,#42038,#42039,#42040,#42041,#42042,
#42043,#42044,#42045,#42046,#42047,#42048,#42049,#42050,#42051,#42052,#42053,
#42054,#42055,#42056,#42057,#42058,#42059,#42060,#42061,#42062,#42063,#42064,
#42065,#42066,#42067,#42068,#42069,#42070,#42071,#42072,#42073,#42074,#42075,
#42076,#42077,#42078,#42079,#42080,#42081,#42082,#42083,#42084,#42085,#42086,
#42087,#42088,#42089,#42090,#42091,#42092,#42093,#42094,#42095,#42096,#42097,
#42098,#42099,#42100,#42101),.UNSPECIFIED.,.F.,.F.,(4,3,3,3,3,3,3,3,3,3,
3,3,3,3,3,3,3,3,3,3,3,3,3,3,3,3,3,3,3,3,3,3,3,3,3,3,3,3,3,3,3,3,3,3,3,3,
3,3,3,3,3,3,3,3,3,3,3,3,3,3,3,3,3,3,3,3,3,3,3,3,3,3,3,3,3,3,4),(147.654854718722,
147.741934294221,147.829116802213,147.916493787936,148.003971880025,148.091648447011,
148.163613175116,148.247359907818,148.331003584834,148.414564328901,148.498062190857,
148.58152469142,148.664969826912,148.748415661755,148.831880256993,148.915433442415,
148.999031275988,149.08276283885,149.162596677315,149.246343410017,149.329987087033,
149.413547831099,149.497045693056,149.580508193619,149.663953329111,149.747399163954,
149.830863759193,149.914416944614,149.998014778187,150.081746341049,150.161580179515,
150.245326912217,150.328970589233,150.412531333299,150.496029195256,150.579491695819,
150.662936831311,150.746382666154,150.829847261392,150.913400446814,150.996998280387,
151.080729843248,151.160563681714,151.244310414416,151.327954091431,151.411514835498,
151.495012697454,151.578475198017,151.661920333509,151.745366168352,151.82883076359,
151.912383949012,151.995981782585,152.079713345447,152.159547183913,152.243293916615,
152.326937593631,152.410498337697,152.493996199654,152.577458700216,152.660903835709,
152.744349670551,152.82781426579,152.911367451212,152.994965284784,153.078696847646,
153.158530686112,153.241143602457,153.323652758631,153.406066476268,153.488426755207,
153.570752601881,153.653062991075,153.735403927003,153.817761944655,153.900190984863,
153.938040025744),.UNSPECIFIED.);
#393=B_SPLINE_CURVE_WITH_KNOTS('',3,(#42103,#42104,#42105,#42106,#42107,
#42108,#42109,#42110,#42111,#42112,#42113,#42114,#42115,#42116,#42117,#42118,
#42119,#42120,#42121,#42122,#42123,#42124,#42125,#42126,#42127,#42128,#42129,
#42130,#42131,#42132,#42133,#42134,#42135,#42136,#42137,#42138,#42139,#42140,
#42141,#42142,#42143,#42144,#42145,#42146,#42147,#42148,#42149,#42150,#42151,
#42152,#42153,#42154,#42155,#42156,#42157,#42158,#42159,#42160,#42161,#42162,
#42163,#42164,#42165,#42166,#42167,#42168,#42169,#42170,#42171,#42172,#42173,
#42174,#42175,#42176,#42177,#42178,#42179,#42180,#42181,#42182,#42183,#42184,
#42185,#42186,#42187,#42188,#42189,#42190,#42191,#42192,#42193,#42194,#42195,
#42196,#42197,#42198,#42199,#42200,#42201,#42202,#42203,#42204,#42205,#42206,
#42207,#42208,#42209,#42210,#42211,#42212,#42213,#42214,#42215,#42216,#42217,
#42218,#42219,#42220,#42221,#42222,#42223,#42224,#42225,#42226,#42227,#42228,
#42229,#42230,#42231,#42232,#42233,#42234,#42235,#42236,#42237,#42238,#42239,
#42240,#42241,#42242,#42243,#42244,#42245,#42246,#42247,#42248,#42249,#42250,
#42251,#42252,#42253,#42254,#42255,#42256,#42257,#42258,#42259,#42260,#42261,
#42262,#42263,#42264,#42265,#42266,#42267,#42268,#42269,#42270,#42271,#42272,
#42273,#42274,#42275,#42276,#42277,#42278,#42279,#42280,#42281,#42282,#42283,
#42284,#42285,#42286,#42287,#42288,#42289,#42290,#42291,#42292,#42293,#42294,
#42295,#42296,#42297,#42298,#42299,#42300,#42301,#42302,#42303,#42304,#42305,
#42306,#42307,#42308,#42309,#42310,#42311,#42312,#42313,#42314,#42315,#42316,
#42317,#42318,#42319,#42320,#42321,#42322,#42323,#42324,#42325,#42326,#42327,
#42328,#42329,#42330,#42331),.UNSPECIFIED.,.F.,.F.,(4,3,3,3,3,3,3,3,3,3,
3,3,3,3,3,3,3,3,3,3,3,3,3,3,3,3,3,3,3,3,3,3,3,3,3,3,3,3,3,3,3,3,3,3,3,3,
3,3,3,3,3,3,3,3,3,3,3,3,3,3,3,3,3,3,3,3,3,3,3,3,3,3,3,3,3,3,4),(141.37166951201,
141.454058249237,141.536378431309,141.618656662166,141.700914289754,141.783170319096,
141.865443751679,141.947801446069,142.03020435425,142.112731423433,142.169712161921,
142.253458894623,142.337102571639,142.420663315705,142.504161177662,142.587623678225,
142.671068813717,142.75451464856,142.837979243798,142.92153242922,143.005130262793,
143.088861825655,143.16869566412,143.252442396822,143.336086073838,143.419646817905,
143.503144679862,143.586607180424,143.670052315917,143.75349815076,143.836962745998,
143.92051593142,144.004113764992,144.087845327854,144.16767916632,144.251425899022,
144.335069576038,144.418630320104,144.502128182061,144.585590682624,144.669035818116,
144.752481652958,144.835946248197,144.919499433619,145.003097267191,145.086828830053,
145.166662668519,145.250409401221,145.334053078237,145.417613822303,145.50111168426,
145.584574184822,145.668019320314,145.751465155157,145.834929750395,145.918482935817,
146.002080769389,146.085812332251,146.165646170718,146.24939290342,146.333036580436,
146.416597324503,146.50009518646,146.583557687022,146.667002822515,146.750448657358,
146.833913252596,146.917466438018,147.00106427159,147.084795834452,147.164629672917,
147.253060978591,147.341334586321,147.429396673395,147.517331621313,147.605097658525,
147.654854718538),.UNSPECIFIED.);
#394=B_SPLINE_CURVE_WITH_KNOTS('',3,(#42333,#42334,#42335,#42336,#42337,
#42338,#42339,#42340,#42341,#42342,#42343),.UNSPECIFIED.,.F.,.F.,(4,1,1,
1,1,1,1,1,4),(135.088484104363,135.176827646527,136.175811148726,137.174794650925,
138.173778153125,139.172761655324,140.171745157523,141.170728659722,141.371669411542),
 .UNSPECIFIED.);
#395=B_SPLINE_CURVE_WITH_KNOTS('',3,(#42345,#42346,#42347,#42348,#42349,
#42350,#42351,#42352,#42353,#42354,#42355,#42356,#42357,#42358,#42359,#42360,
#42361,#42362,#42363,#42364,#42365,#42366,#42367,#42368,#42369,#42370,#42371,
#42372,#42373,#42374,#42375,#42376,#42377,#42378,#42379,#42380,#42381,#42382,
#42383,#42384,#42385,#42386,#42387,#42388,#42389,#42390,#42391,#42392,#42393,
#42394,#42395,#42396,#42397,#42398,#42399,#42400,#42401,#42402,#42403,#42404,
#42405,#42406,#42407,#42408,#42409,#42410,#42411,#42412,#42413,#42414,#42415,
#42416,#42417,#42418,#42419,#42420,#42421,#42422,#42423,#42424,#42425,#42426,
#42427,#42428,#42429,#42430,#42431,#42432,#42433,#42434,#42435,#42436,#42437,
#42438,#42439,#42440,#42441,#42442,#42443,#42444,#42445,#42446,#42447,#42448,
#42449,#42450,#42451,#42452,#42453,#42454,#42455,#42456,#42457,#42458,#42459,
#42460,#42461,#42462,#42463,#42464,#42465,#42466,#42467,#42468,#42469,#42470,
#42471,#42472,#42473,#42474,#42475,#42476,#42477,#42478,#42479,#42480,#42481,
#42482,#42483,#42484,#42485,#42486,#42487,#42488,#42489,#42490,#42491,#42492,
#42493,#42494,#42495,#42496,#42497,#42498,#42499,#42500,#42501,#42502,#42503,
#42504,#42505,#42506,#42507,#42508,#42509,#42510,#42511,#42512,#42513,#42514,
#42515,#42516,#42517,#42518,#42519,#42520,#42521,#42522,#42523,#42524,#42525,
#42526,#42527,#42528,#42529,#42530,#42531,#42532,#42533,#42534,#42535,#42536,
#42537,#42538,#42539,#42540,#42541,#42542,#42543,#42544,#42545,#42546,#42547,
#42548,#42549,#42550,#42551,#42552,#42553,#42554,#42555,#42556,#42557,#42558,
#42559,#42560,#42561,#42562,#42563,#42564,#42565,#42566,#42567,#42568,#42569,
#42570),.UNSPECIFIED.,.F.,.F.,(4,3,3,3,3,3,3,3,3,3,3,3,3,3,3,3,3,3,3,3,
3,3,3,3,3,3,3,3,3,3,3,3,3,3,3,3,3,3,3,3,3,3,3,3,3,3,3,3,3,3,3,3,3,3,3,3,
3,3,3,3,3,3,3,3,3,3,3,3,3,3,3,3,3,3,3,4),(128.805298797375,128.899705756365,
128.993788658939,129.088376322271,129.182926633332,129.266673366034,129.350317043049,
129.433877787116,129.517375649072,129.600838149635,129.684283285127,129.76772911997,
129.851193715207,129.934746900629,130.018344734202,130.102076297063,130.181910135531,
130.265656868233,130.349300545249,130.432861289315,130.516359151272,130.599821651835,
130.683266787327,130.76671262217,130.850177217408,130.93373040283,131.017328236403,
131.101059799265,131.18089363773,131.264640370432,131.348284047448,131.431844791514,
131.515342653471,131.598805154033,131.682250289526,131.765696124368,131.849160719606,
131.932713905028,132.016311738601,132.100043301463,132.17987713993,132.263623872632,
132.347267549648,132.430828293715,132.514326155671,132.597788656234,132.681233791727,
132.764679626569,132.848144221808,132.93169740723,133.015295240802,133.099026803664,
133.178860642129,133.262607374831,133.346251051847,133.429811795913,133.51330965787,
133.596772158432,133.680217293925,133.763663128767,133.847127724005,133.930680909427,
134.014278743,134.098010305862,134.177844144328,134.26061799334,134.343289547075,
134.425879829208,134.508705328763,134.591202397923,134.67368585154,134.756174542847,
134.839251863547,134.921846228862,135.005165027255,135.088483825647),
 .UNSPECIFIED.);
#396=B_SPLINE_CURVE_WITH_KNOTS('',3,(#42572,#42573,#42574,#42575,#42576,
#42577,#42578,#42579,#42580,#42581,#42582,#42583,#42584,#42585,#42586,#42587,
#42588,#42589,#42590,#42591,#42592,#42593,#42594,#42595,#42596,#42597,#42598,
#42599,#42600,#42601,#42602,#42603,#42604,#42605,#42606,#42607,#42608,#42609,
#42610,#42611,#42612,#42613,#42614,#42615,#42616,#42617,#42618,#42619,#42620,
#42621,#42622,#42623,#42624,#42625,#42626,#42627,#42628,#42629,#42630,#42631,
#42632,#42633,#42634,#42635,#42636,#42637,#42638,#42639,#42640,#42641,#42642,
#42643,#42644,#42645,#42646,#42647,#42648,#42649,#42650,#42651,#42652,#42653,
#42654,#42655,#42656,#42657,#42658,#42659,#42660,#42661,#42662,#42663,#42664,
#42665,#42666,#42667,#42668,#42669,#42670,#42671,#42672,#42673,#42674,#42675,
#42676,#42677,#42678,#42679,#42680,#42681,#42682,#42683,#42684,#42685,#42686,
#42687,#42688,#42689,#42690,#42691,#42692,#42693,#42694,#42695,#42696,#42697,
#42698,#42699,#42700,#42701,#42702,#42703,#42704,#42705,#42706,#42707,#42708,
#42709,#42710,#42711,#42712,#42713,#42714,#42715,#42716,#42717,#42718,#42719,
#42720,#42721,#42722,#42723,#42724,#42725,#42726,#42727,#42728,#42729,#42730,
#42731,#42732,#42733,#42734,#42735,#42736,#42737,#42738,#42739,#42740,#42741,
#42742,#42743,#42744,#42745,#42746,#42747,#42748,#42749,#42750,#42751,#42752,
#42753,#42754,#42755,#42756,#42757,#42758,#42759,#42760,#42761,#42762,#42763,
#42764,#42765,#42766,#42767,#42768,#42769,#42770,#42771,#42772,#42773,#42774,
#42775,#42776,#42777,#42778,#42779,#42780,#42781,#42782,#42783,#42784,#42785,
#42786,#42787,#42788,#42789,#42790,#42791,#42792,#42793,#42794,#42795,#42796,
#42797,#42798,#42799,#42800),.UNSPECIFIED.,.F.,.F.,(4,3,3,3,3,3,3,3,3,3,
3,3,3,3,3,3,3,3,3,3,3,3,3,3,3,3,3,3,3,3,3,3,3,3,3,3,3,3,3,3,3,3,3,3,3,3,
3,3,3,3,3,3,3,3,3,3,3,3,3,3,3,3,3,3,3,3,3,3,3,3,3,3,3,3,3,3,4),(122.522113490004,
122.605495334217,122.688863359942,122.772235636009,122.855630230272,122.93911972146,
123.022656907832,123.106334733695,123.189025620137,123.272772352839,123.356416029855,
123.439976773921,123.523474635878,123.606937136441,123.690382271933,123.773828106776,
123.857292702013,123.940845887435,124.024443721008,124.10817528387,124.188009122336,
124.271755855038,124.355399532054,124.43896027612,124.522458138077,124.60592063864,
124.689365774132,124.772811608975,124.856276204213,124.939829389635,125.023427223208,
125.10715878607,125.186992624535,125.270739357237,125.354383034253,125.437943778319,
125.521441640276,125.604904140838,125.688349276331,125.771795111174,125.855259706412,
125.938812891834,126.022410725406,126.106142288268,126.185976126735,126.269722859437,
126.353366536453,126.436927280519,126.520425142477,126.603887643039,126.687332778532,
126.770778613374,126.854243208613,126.937796394035,127.021394227608,127.10512579047,
127.184959628934,127.268706361636,127.352350038652,127.435910782718,127.519408644675,
127.602871145237,127.68631628073,127.769762115572,127.85322671081,127.936779896232,
128.020377729805,128.104109292666,128.183943131133,128.268438217603,128.352825675139,
128.437122797182,128.521346811719,128.605510027022,128.689637939473,128.773753455852,
128.805298797183),.UNSPECIFIED.);
#397=B_SPLINE_CURVE_WITH_KNOTS('',3,(#42802,#42803,#42804,#42805,#42806,
#42807,#42808,#42809,#42810,#42811,#42812,#42813,#42814,#42815,#42816,#42817,
#42818,#42819,#42820,#42821,#42822,#42823,#42824,#42825,#42826,#42827,#42828,
#42829,#42830,#42831,#42832,#42833,#42834,#42835,#42836,#42837,#42838,#42839,
#42840,#42841,#42842,#42843,#42844,#42845,#42846,#42847,#42848,#42849,#42850,
#42851,#42852,#42853,#42854,#42855,#42856,#42857,#42858,#42859,#42860,#42861,
#42862,#42863,#42864,#42865,#42866,#42867,#42868,#42869,#42870,#42871,#42872,
#42873,#42874,#42875,#42876,#42877,#42878,#42879,#42880,#42881,#42882,#42883,
#42884,#42885,#42886,#42887,#42888,#42889,#42890,#42891,#42892,#42893,#42894,
#42895,#42896,#42897,#42898,#42899,#42900,#42901,#42902,#42903,#42904,#42905,
#42906,#42907,#42908,#42909,#42910,#42911,#42912,#42913,#42914,#42915,#42916,
#42917,#42918,#42919,#42920,#42921,#42922,#42923,#42924,#42925,#42926,#42927,
#42928,#42929,#42930,#42931,#42932,#42933,#42934,#42935,#42936,#42937,#42938,
#42939,#42940,#42941,#42942,#42943,#42944,#42945,#42946,#42947,#42948,#42949,
#42950,#42951,#42952,#42953,#42954,#42955,#42956,#42957,#42958,#42959,#42960,
#42961,#42962,#42963,#42964,#42965,#42966,#42967,#42968,#42969,#42970,#42971,
#42972,#42973,#42974,#42975,#42976,#42977,#42978,#42979,#42980,#42981,#42982,
#42983,#42984,#42985,#42986,#42987,#42988,#42989,#42990,#42991,#42992,#42993,
#42994,#42995,#42996,#42997,#42998,#42999,#43000,#43001,#43002,#43003,#43004,
#43005,#43006,#43007,#43008,#43009,#43010,#43011,#43012,#43013,#43014,#43015,
#43016,#43017,#43018,#43019,#43020,#43021,#43022,#43023,#43024,#43025,#43026,
#43027,#43028,#43029,#43030),.UNSPECIFIED.,.F.,.F.,(4,3,3,3,3,3,3,3,3,3,
3,3,3,3,3,3,3,3,3,3,3,3,3,3,3,3,3,3,3,3,3,3,3,3,3,3,3,3,3,3,3,3,3,3,3,3,
3,3,3,3,3,3,3,3,3,3,3,3,3,3,3,3,3,3,3,3,3,3,3,3,3,3,3,3,3,3,4),(116.238928183001,
116.322101803165,116.405174762509,116.488167733349,116.57110131169,116.654004557597,
116.736894597209,116.819789987459,116.902709285658,116.985718066432,117.068777060043,
117.151958344376,117.195124606942,117.278871339644,117.36251501666,117.446075760727,
117.529573622683,117.613036123246,117.696481258738,117.779927093581,117.863391688819,
117.946944874241,118.030542707814,118.114274270676,118.194108109141,118.277854841843,
118.361498518859,118.445059262926,118.528557124882,118.612019625445,118.695464760937,
118.77891059578,118.862375191018,118.94592837644,119.029526210013,119.113257772875,
119.193091611341,119.276838344043,119.360482021059,119.444042765125,119.527540627082,
119.611003127645,119.694448263137,119.77789409798,119.861358693218,119.94491187864,
120.028509712213,120.112241275075,120.19207511354,120.275821846242,120.359465523258,
120.443026267324,120.526524129281,120.609986629844,120.693431765336,120.776877600179,
120.860342195416,120.943895380838,121.027493214411,121.111224777272,121.191058615739,
121.274805348441,121.358449025457,121.442009769523,121.52550763148,121.608970132042,
121.692415267535,121.775861102378,121.859325697616,121.942878883038,122.026476716611,
122.110208279473,122.190042117938,122.288536143836,122.386570282577,122.483756133139,
122.522113489818),.UNSPECIFIED.);
#398=B_SPLINE_CURVE_WITH_KNOTS('',3,(#43032,#43033,#43034,#43035,#43036,
#43037,#43038,#43039,#43040,#43041,#43042,#43043,#43044,#43045,#43046,#43047,
#43048,#43049,#43050,#43051,#43052,#43053,#43054,#43055,#43056,#43057,#43058,
#43059,#43060,#43061,#43062,#43063,#43064,#43065,#43066,#43067,#43068,#43069,
#43070,#43071,#43072,#43073,#43074,#43075,#43076,#43077,#43078,#43079,#43080,
#43081,#43082,#43083,#43084,#43085,#43086,#43087,#43088,#43089,#43090,#43091,
#43092,#43093,#43094,#43095,#43096,#43097,#43098,#43099,#43100,#43101,#43102,
#43103,#43104,#43105,#43106,#43107,#43108,#43109,#43110,#43111,#43112,#43113,
#43114,#43115,#43116,#43117,#43118,#43119,#43120,#43121,#43122,#43123,#43124,
#43125,#43126,#43127,#43128,#43129,#43130,#43131,#43132,#43133,#43134,#43135,
#43136,#43137,#43138,#43139,#43140,#43141,#43142,#43143,#43144,#43145,#43146,
#43147,#43148,#43149,#43150,#43151,#43152,#43153,#43154,#43155,#43156,#43157,
#43158,#43159,#43160,#43161,#43162,#43163,#43164,#43165,#43166,#43167,#43168,
#43169,#43170,#43171,#43172,#43173,#43174,#43175,#43176,#43177,#43178,#43179,
#43180,#43181,#43182,#43183,#43184,#43185,#43186,#43187,#43188,#43189,#43190,
#43191,#43192,#43193,#43194,#43195,#43196,#43197,#43198,#43199,#43200,#43201,
#43202,#43203,#43204,#43205,#43206,#43207,#43208,#43209,#43210,#43211,#43212,
#43213,#43214,#43215,#43216,#43217,#43218,#43219,#43220,#43221,#43222,#43223,
#43224,#43225,#43226,#43227,#43228,#43229,#43230,#43231,#43232,#43233,#43234,
#43235,#43236,#43237,#43238,#43239,#43240,#43241,#43242,#43243,#43244,#43245,
#43246,#43247,#43248,#43249,#43250,#43251,#43252,#43253,#43254,#43255,#43256,
#43257,#43258,#43259,#43260),.UNSPECIFIED.,.F.,.F.,(4,3,3,3,3,3,3,3,3,3,
3,3,3,3,3,3,3,3,3,3,3,3,3,3,3,3,3,3,3,3,3,3,3,3,3,3,3,3,3,3,3,3,3,3,3,3,
3,3,3,3,3,3,3,3,3,3,3,3,3,3,3,3,3,3,3,3,3,3,3,3,3,3,3,3,3,3,4),(109.955742875786,
110.063488503129,110.17374886387,110.202240091548,110.28598682425,110.369630501266,
110.453191245332,110.536689107289,110.620151607852,110.703596743344,110.787042578187,
110.870507173425,110.954060358847,111.03765819242,111.121389755281,111.201223593747,
111.284970326449,111.368614003465,111.452174747531,111.535672609488,111.619135110051,
111.702580245543,111.786026080386,111.869490675624,111.953043861046,112.036641694618,
112.12037325748,112.200207095946,112.283953828648,112.367597505664,112.451158249731,
112.534656111687,112.61811861225,112.701563747742,112.785009582585,112.868474177823,
112.952027363245,113.035625196818,113.11935675968,113.199190598146,113.282937330848,
113.366581007864,113.45014175193,113.533639613887,113.61710211445,113.700547249942,
113.783993084785,113.867457680023,113.951010865445,114.034608699017,114.118340261879,
114.198174100345,114.281920833047,114.365564510063,114.449125254129,114.532623116086,
114.616085616648,114.699530752141,114.782976586983,114.866441182221,114.949994367643,
115.033592201216,115.117323764077,115.197157602544,115.280904335246,115.364548012262,
115.448108756328,115.531606618285,115.615069118848,115.69851425434,115.781960089183,
115.865424684421,115.948977869843,116.032575703416,116.116307266278,116.196141104743,
116.238928182824),.UNSPECIFIED.);
#399=B_SPLINE_CURVE_WITH_KNOTS('',3,(#43262,#43263,#43264,#43265,#43266,
#43267,#43268,#43269,#43270,#43271,#43272,#43273,#43274,#43275,#43276,#43277,
#43278,#43279,#43280,#43281,#43282,#43283,#43284,#43285,#43286,#43287,#43288,
#43289,#43290,#43291,#43292,#43293,#43294,#43295,#43296,#43297,#43298,#43299,
#43300,#43301,#43302,#43303,#43304,#43305,#43306,#43307,#43308,#43309,#43310,
#43311,#43312,#43313,#43314,#43315,#43316,#43317,#43318,#43319,#43320,#43321,
#43322,#43323,#43324,#43325,#43326,#43327,#43328,#43329,#43330,#43331,#43332,
#43333,#43334,#43335,#43336,#43337,#43338,#43339,#43340,#43341,#43342,#43343,
#43344,#43345,#43346,#43347,#43348,#43349,#43350,#43351,#43352,#43353,#43354,
#43355,#43356,#43357,#43358,#43359,#43360,#43361,#43362,#43363,#43364,#43365,
#43366,#43367,#43368,#43369,#43370,#43371,#43372,#43373,#43374,#43375,#43376,
#43377,#43378,#43379,#43380,#43381,#43382,#43383,#43384,#43385,#43386,#43387,
#43388,#43389,#43390,#43391,#43392,#43393,#43394,#43395,#43396,#43397,#43398,
#43399,#43400,#43401,#43402,#43403,#43404,#43405,#43406,#43407,#43408,#43409,
#43410,#43411,#43412,#43413,#43414,#43415,#43416,#43417,#43418,#43419,#43420,
#43421,#43422,#43423,#43424,#43425,#43426,#43427,#43428,#43429,#43430,#43431,
#43432,#43433,#43434,#43435,#43436,#43437,#43438,#43439,#43440,#43441,#43442,
#43443,#43444,#43445,#43446,#43447,#43448,#43449,#43450,#43451,#43452,#43453,
#43454,#43455,#43456,#43457,#43458,#43459,#43460,#43461,#43462,#43463,#43464,
#43465,#43466,#43467,#43468,#43469,#43470,#43471,#43472,#43473,#43474,#43475,
#43476,#43477,#43478,#43479,#43480,#43481,#43482,#43483,#43484,#43485,#43486,
#43487,#43488,#43489,#43490),.UNSPECIFIED.,.F.,.F.,(4,3,3,3,3,3,3,3,3,3,
3,3,3,3,3,3,3,3,3,3,3,3,3,3,3,3,3,3,3,3,3,3,3,3,3,3,3,3,3,3,3,3,3,3,3,3,
3,3,3,3,3,3,3,3,3,3,3,3,3,3,3,3,3,3,3,3,3,3,3,3,3,3,3,3,3,3,4),(103.672557568465,
103.758762666372,103.845040757771,103.935865337916,104.022392995456,104.109013779931,
104.195789661329,104.208339078353,104.292085811055,104.375729488071,104.459290232137,
104.542788094094,104.626250594656,104.709695730149,104.793141564991,104.876606160229,
104.960159345651,105.043757179224,105.127488742085,105.207322580552,105.291069313254,
105.37471299027,105.458273734336,105.541771596293,105.625234096856,105.708679232348,
105.792125067191,105.875589662429,105.959142847851,106.042740681423,106.126472244285,
106.206306082751,106.290052815453,106.373696492469,106.457257236535,106.540755098492,
106.624217599055,106.707662734547,106.79110856939,106.874573164628,106.95812635005,
107.041724183623,107.125455746485,107.205289584951,107.289036317653,107.372679994669,
107.456240738735,107.539738600692,107.623201101255,107.706646236747,107.79009207159,
107.873556666828,107.95710985225,108.040707685822,108.124439248684,108.20427308715,
108.288019819852,108.371663496868,108.455224240934,108.538722102891,108.622184603453,
108.705629738945,108.789075573788,108.872540169026,108.956093354448,109.03969118802,
109.123422750882,109.203256589349,109.286024516412,109.369739311316,109.452303664454,
109.534813329928,109.617287215932,109.70190113086,109.784381810341,109.870062342993,
109.955742875645),.UNSPECIFIED.);
#400=B_SPLINE_CURVE_WITH_KNOTS('',3,(#43492,#43493,#43494,#43495,#43496,
#43497,#43498,#43499,#43500,#43501,#43502,#43503,#43504,#43505,#43506,#43507,
#43508,#43509,#43510,#43511,#43512,#43513,#43514,#43515,#43516,#43517,#43518,
#43519,#43520,#43521,#43522,#43523,#43524,#43525,#43526,#43527,#43528,#43529,
#43530,#43531,#43532,#43533,#43534,#43535,#43536,#43537,#43538,#43539,#43540,
#43541,#43542,#43543,#43544,#43545,#43546,#43547,#43548,#43549,#43550,#43551,
#43552,#43553,#43554,#43555,#43556,#43557,#43558,#43559,#43560,#43561,#43562,
#43563,#43564,#43565,#43566,#43567,#43568,#43569,#43570,#43571,#43572,#43573,
#43574,#43575,#43576,#43577,#43578,#43579,#43580,#43581,#43582,#43583,#43584,
#43585,#43586,#43587,#43588,#43589,#43590,#43591,#43592,#43593,#43594,#43595,
#43596,#43597,#43598,#43599,#43600,#43601,#43602,#43603,#43604,#43605,#43606,
#43607,#43608,#43609,#43610,#43611,#43612,#43613,#43614,#43615,#43616,#43617,
#43618,#43619,#43620,#43621,#43622,#43623,#43624,#43625,#43626,#43627,#43628,
#43629,#43630,#43631,#43632,#43633,#43634,#43635,#43636,#43637,#43638,#43639,
#43640,#43641,#43642,#43643,#43644,#43645,#43646,#43647,#43648,#43649,#43650,
#43651,#43652,#43653,#43654,#43655,#43656,#43657,#43658,#43659,#43660,#43661,
#43662,#43663,#43664,#43665,#43666,#43667,#43668,#43669,#43670,#43671,#43672,
#43673,#43674,#43675,#43676,#43677,#43678,#43679,#43680,#43681,#43682,#43683,
#43684,#43685,#43686,#43687,#43688,#43689,#43690,#43691,#43692,#43693,#43694,
#43695,#43696,#43697,#43698,#43699,#43700,#43701,#43702,#43703,#43704,#43705,
#43706,#43707,#43708,#43709,#43710,#43711,#43712,#43713,#43714,#43715,#43716,
#43717,#43718,#43719,#43720),.UNSPECIFIED.,.F.,.F.,(4,3,3,3,3,3,3,3,3,3,
3,3,3,3,3,3,3,3,3,3,3,3,3,3,3,3,3,3,3,3,3,3,3,3,3,3,3,3,3,3,3,3,3,3,3,3,
3,3,3,3,3,3,3,3,3,3,3,3,3,3,3,3,3,3,3,3,3,3,3,3,3,3,3,3,3,3,4),(97.389372261456,
97.4717475320007,97.554046784624,97.6365956946908,97.718815685072,97.8010275054444,
97.8832501830832,97.9660471536019,98.0483900879616,98.1314140765598,98.214438065158,
98.2981847978599,98.3818284748756,98.4653892189419,98.5488870808986,98.6323495814612,
98.7157947169534,98.7992405517961,98.8827051470339,98.9662583324558,99.0498561660283,
99.1335877288901,99.2134215673572,99.2971683000592,99.380811977075,99.4643727211417,
99.5478705830985,99.6313330836612,99.7147782191535,99.7982240539964,99.8816886492344,
99.9652418346564,100.048839668229,100.132571231091,100.212405069556,100.296151802258,
100.379795479274,100.46335622334,100.546854085297,100.630316585859,100.713761721352,
100.797207556195,100.880672151433,100.964225336855,101.047823170427,101.131554733289,
101.211388571756,101.295135304458,101.378778981474,101.46233972554,101.545837587497,
101.629300088059,101.712745223552,101.796191058395,101.879655653632,101.963208839054,
102.046806672627,102.130538235489,102.210372073955,102.294118806657,102.377762483673,
102.46132322774,102.544821089696,102.628283590259,102.711728725751,102.795174560593,
102.878639155831,102.962192341253,103.045790174826,103.129521737688,103.209355576154,
103.298982946675,103.392376602082,103.481568554493,103.570604407169,103.659433763089,
103.672557568303),.UNSPECIFIED.);
#401=B_SPLINE_CURVE_WITH_KNOTS('',3,(#43722,#43723,#43724,#43725,#43726,
#43727,#43728,#43729,#43730,#43731,#43732,#43733,#43734,#43735,#43736,#43737,
#43738,#43739,#43740,#43741,#43742,#43743,#43744,#43745,#43746,#43747,#43748,
#43749,#43750,#43751,#43752,#43753,#43754,#43755,#43756,#43757,#43758,#43759,
#43760,#43761,#43762,#43763,#43764,#43765,#43766,#43767,#43768,#43769,#43770,
#43771,#43772,#43773,#43774,#43775,#43776,#43777,#43778,#43779,#43780,#43781,
#43782,#43783,#43784,#43785,#43786,#43787,#43788,#43789,#43790,#43791,#43792,
#43793,#43794,#43795,#43796,#43797,#43798,#43799,#43800,#43801,#43802,#43803,
#43804,#43805,#43806,#43807,#43808,#43809,#43810,#43811,#43812,#43813,#43814,
#43815,#43816,#43817,#43818,#43819,#43820,#43821,#43822,#43823,#43824,#43825,
#43826,#43827,#43828,#43829,#43830,#43831,#43832,#43833,#43834,#43835,#43836,
#43837,#43838,#43839,#43840,#43841,#43842,#43843,#43844,#43845,#43846,#43847,
#43848,#43849,#43850,#43851,#43852,#43853,#43854,#43855,#43856,#43857,#43858,
#43859,#43860,#43861,#43862,#43863,#43864,#43865,#43866,#43867,#43868,#43869,
#43870,#43871,#43872,#43873,#43874,#43875,#43876,#43877,#43878,#43879,#43880,
#43881,#43882,#43883,#43884,#43885,#43886,#43887,#43888,#43889,#43890,#43891,
#43892,#43893,#43894,#43895,#43896,#43897,#43898,#43899,#43900,#43901,#43902,
#43903,#43904,#43905,#43906,#43907,#43908,#43909,#43910,#43911,#43912,#43913,
#43914,#43915,#43916,#43917,#43918,#43919,#43920,#43921,#43922,#43923,#43924,
#43925,#43926,#43927,#43928,#43929,#43930,#43931,#43932,#43933,#43934,#43935,
#43936,#43937,#43938,#43939,#43940,#43941,#43942,#43943,#43944,#43945,#43946,
#43947),.UNSPECIFIED.,.F.,.F.,(4,3,3,3,3,3,3,3,3,3,3,3,3,3,3,3,3,3,3,3,
3,3,3,3,3,3,3,3,3,3,3,3,3,3,3,3,3,3,3,3,3,3,3,3,3,3,3,3,3,3,3,3,3,3,3,3,
3,3,3,3,3,3,3,3,3,3,3,3,3,3,3,3,3,3,3,4),(91.1061869541058,91.2215535497639,
91.3053002824658,91.3889439594816,91.4725047035478,91.5560025655045,91.6394650660671,
91.7229102015593,91.8063560364022,91.8898206316402,91.9733738170621,92.0569716506346,
92.1407032134965,92.220537051963,92.304283784665,92.3879274616808,92.4714882057472,
92.5549860677039,92.6384485682665,92.7218937037588,92.8053395386016,92.8888041338397,
92.9723573192615,93.0559551528342,93.139686715696,93.2195205541622,93.3032672868643,
93.3869109638802,93.4704717079468,93.5539695699036,93.6374320704662,93.7208772059586,
93.8043230408015,93.8877876360397,93.9713408214616,94.0549386550344,94.1386702178963,
94.2185040563614,94.3022507890633,94.385894466079,94.4694552101454,94.552953072102,
94.6364155726645,94.7198607081567,94.8033065429994,94.8867711382374,94.9703243236592,
95.0539221572317,95.1376537200934,95.2174875585605,95.3012342912625,95.3848779682784,
95.4684387123449,95.5519365743017,95.6353990748643,95.7188442103567,95.8022900451996,
95.8857546404377,95.9693078258596,96.0529056594323,96.1366372222942,96.2164710607597,
96.3002177934616,96.3838614704774,96.467422214544,96.5509200765008,96.6343825770633,
96.7178277125556,96.8012735473983,96.8847381426364,96.9682913280583,97.0518891616309,
97.1356207244927,97.2154545629589,97.3450039787278,97.3893722612854),
 .UNSPECIFIED.);
#402=B_SPLINE_CURVE_WITH_KNOTS('',3,(#43949,#43950,#43951,#43952,#43953,
#43954,#43955,#43956,#43957,#43958,#43959,#43960,#43961,#43962,#43963,#43964,
#43965,#43966,#43967,#43968,#43969,#43970,#43971,#43972,#43973,#43974,#43975,
#43976,#43977,#43978,#43979,#43980,#43981,#43982,#43983,#43984,#43985,#43986,
#43987,#43988,#43989,#43990,#43991,#43992,#43993,#43994,#43995,#43996,#43997,
#43998,#43999,#44000,#44001,#44002,#44003,#44004,#44005,#44006,#44007,#44008,
#44009,#44010,#44011,#44012,#44013,#44014,#44015,#44016,#44017,#44018,#44019,
#44020,#44021,#44022,#44023,#44024,#44025,#44026,#44027,#44028,#44029,#44030,
#44031,#44032,#44033,#44034,#44035,#44036,#44037,#44038,#44039,#44040,#44041,
#44042,#44043,#44044,#44045,#44046,#44047,#44048,#44049,#44050,#44051,#44052,
#44053,#44054,#44055,#44056,#44057,#44058,#44059,#44060,#44061,#44062,#44063,
#44064,#44065,#44066,#44067,#44068,#44069,#44070,#44071,#44072,#44073,#44074,
#44075,#44076,#44077,#44078,#44079,#44080,#44081,#44082,#44083,#44084,#44085,
#44086,#44087,#44088,#44089,#44090,#44091,#44092,#44093,#44094,#44095,#44096,
#44097,#44098,#44099,#44100,#44101,#44102,#44103,#44104,#44105,#44106,#44107,
#44108,#44109,#44110,#44111,#44112,#44113,#44114,#44115,#44116,#44117,#44118,
#44119,#44120,#44121,#44122,#44123,#44124,#44125,#44126,#44127,#44128,#44129,
#44130,#44131,#44132,#44133,#44134,#44135,#44136,#44137,#44138,#44139,#44140,
#44141,#44142,#44143,#44144,#44145,#44146,#44147,#44148,#44149,#44150,#44151,
#44152,#44153,#44154,#44155,#44156,#44157,#44158,#44159,#44160,#44161,#44162,
#44163,#44164,#44165,#44166,#44167,#44168,#44169,#44170,#44171,#44172,#44173,
#44174,#44175,#44176,#44177),.UNSPECIFIED.,.F.,.F.,(4,3,3,3,3,3,3,3,3,3,
3,3,3,3,3,3,3,3,3,3,3,3,3,3,3,3,3,3,3,3,3,3,3,3,3,3,3,3,3,3,3,3,3,3,3,3,
3,3,3,3,3,3,3,3,3,3,3,3,3,3,3,3,3,3,3,3,3,3,3,3,3,3,3,3,3,3,4),(84.8230016470981,
84.9147924149001,85.0070556960825,85.0995627342371,85.1923976742333,85.2276525365689,
85.3113992692709,85.3950429462865,85.4786036903529,85.5621015523098,85.6455640528723,
85.7290091883646,85.8124550232074,85.8959196184455,85.9794728038673,86.0630706374399,
86.1468022003017,86.226636038768,86.31038277147,86.3940264484858,86.4775871925524,
86.5610850545091,86.6445475550717,86.727992690564,86.8114385254069,86.894903120645,
86.9784563060669,87.0620541396396,87.1457857025015,87.2256195409672,87.3093662736691,
87.3930099506848,87.4765706947512,87.5600685567078,87.6435310572704,87.7269761927626,
87.8104220276053,87.8938866228433,87.9774398082651,88.0610376418377,88.1447692046995,
88.2246030431664,88.3083497758684,88.3919934528843,88.4755541969509,88.5590520589077,
88.6425145594703,88.7259596949627,88.8094055298056,88.8928701250438,88.9764233104657,
89.0600211440384,89.1437527069003,89.2235865453655,89.3073332780675,89.3909769550833,
89.4745376991498,89.5580355611065,89.6414980616691,89.7249431971614,89.8083890320042,
89.8918536272423,89.9754068126641,90.0590046462367,90.1427362090986,90.2225700475647,
90.3051881406199,90.3877040229452,90.4701388369267,90.5525127567424,90.6348543732513,
90.7171826531799,90.7995165497718,90.8819169921766,90.9643524122932,91.0468970494953,
91.106186953972),.UNSPECIFIED.);
#403=B_SPLINE_CURVE_WITH_KNOTS('',3,(#44179,#44180,#44181,#44182,#44183,
#44184,#44185,#44186,#44187,#44188,#44189,#44190,#44191,#44192,#44193,#44194,
#44195,#44196,#44197,#44198,#44199,#44200,#44201,#44202,#44203,#44204,#44205,
#44206,#44207,#44208,#44209,#44210,#44211,#44212,#44213,#44214,#44215,#44216,
#44217,#44218,#44219,#44220,#44221,#44222,#44223,#44224,#44225,#44226,#44227,
#44228,#44229,#44230,#44231,#44232,#44233,#44234,#44235,#44236,#44237,#44238,
#44239,#44240,#44241,#44242,#44243,#44244,#44245,#44246,#44247,#44248,#44249,
#44250,#44251,#44252,#44253,#44254,#44255,#44256,#44257,#44258,#44259,#44260,
#44261,#44262,#44263,#44264,#44265,#44266,#44267,#44268,#44269,#44270,#44271,
#44272,#44273,#44274,#44275,#44276,#44277,#44278,#44279,#44280,#44281,#44282,
#44283,#44284,#44285,#44286,#44287,#44288,#44289,#44290,#44291,#44292,#44293,
#44294,#44295,#44296,#44297,#44298,#44299,#44300,#44301,#44302,#44303,#44304,
#44305,#44306,#44307,#44308,#44309,#44310,#44311,#44312,#44313,#44314,#44315,
#44316,#44317,#44318,#44319,#44320,#44321,#44322,#44323,#44324,#44325,#44326,
#44327,#44328,#44329,#44330,#44331,#44332,#44333,#44334,#44335,#44336,#44337,
#44338,#44339,#44340,#44341,#44342,#44343,#44344,#44345,#44346,#44347,#44348,
#44349,#44350,#44351,#44352,#44353,#44354,#44355,#44356,#44357,#44358,#44359,
#44360,#44361,#44362,#44363,#44364,#44365,#44366,#44367,#44368,#44369,#44370,
#44371,#44372,#44373,#44374,#44375,#44376,#44377,#44378,#44379,#44380,#44381,
#44382,#44383,#44384,#44385,#44386,#44387,#44388,#44389,#44390,#44391,#44392,
#44393,#44394,#44395,#44396,#44397,#44398,#44399,#44400,#44401,#44402,#44403,
#44404,#44405,#44406,#44407),.UNSPECIFIED.,.F.,.F.,(4,3,3,3,3,3,3,3,3,3,
3,3,3,3,3,3,3,3,3,3,3,3,3,3,3,3,3,3,3,3,3,3,3,3,3,3,3,3,3,3,3,3,3,3,3,3,
3,3,3,3,3,3,3,3,3,3,3,3,3,3,3,3,3,3,3,3,3,3,3,3,3,3,3,3,3,3,4),(78.5398163397466,
78.6265582377,78.7095749161233,78.7925857145311,78.8756090555744,78.9586633669885,
79.0418131756962,79.1250192064087,79.208346008455,79.2337515233739,79.3174982560759,
79.4011419330917,79.4847026771586,79.5682005391154,79.6516630396781,79.7351081751703,
79.818554010013,79.9020186052512,79.985571790673,80.0691696242457,80.1529011871076,
80.2327350255731,80.3164817582751,80.400125435291,80.4836861793577,80.5671840413144,
80.6506465418771,80.7340916773693,80.8175375122122,80.9010021074502,80.984555292872,
81.0681531264446,81.1518846893065,81.2317185277722,81.3154652604742,81.3991089374899,
81.4826696815565,81.5661675435133,81.649630044076,81.7330751795684,81.8165210144114,
81.8999856096495,81.9835387950714,82.0671366286439,82.1508681915057,82.2307020299714,
82.3144487626733,82.3980924396891,82.4816531837558,82.5651510457127,82.6486135462753,
82.7320586817676,82.8155045166105,82.8989691118484,82.9825222972702,83.0661201308428,
83.1498516937047,83.2296855321705,83.3134322648725,83.3970759418886,83.4806366859552,
83.564134547912,83.6475970484746,83.7310421839668,83.8144880188095,83.8979526140471,
83.9815057994689,84.0651036330417,84.1488351959036,84.2286690343697,84.3137666968213,
84.3987507891206,84.4836377060624,84.5684786912783,84.6532096453913,84.7381056461587,
84.8230016469262),.UNSPECIFIED.);
#404=B_SPLINE_CURVE_WITH_KNOTS('',3,(#44409,#44410,#44411,#44412,#44413,
#44414,#44415,#44416,#44417,#44418,#44419,#44420,#44421,#44422,#44423,#44424,
#44425,#44426,#44427,#44428,#44429,#44430,#44431,#44432,#44433,#44434,#44435,
#44436,#44437,#44438,#44439,#44440,#44441,#44442,#44443,#44444,#44445,#44446,
#44447,#44448,#44449,#44450,#44451,#44452,#44453,#44454,#44455,#44456,#44457,
#44458,#44459,#44460,#44461,#44462,#44463,#44464,#44465,#44466,#44467,#44468,
#44469,#44470,#44471,#44472,#44473,#44474,#44475,#44476,#44477,#44478,#44479,
#44480,#44481,#44482,#44483,#44484,#44485,#44486,#44487,#44488,#44489,#44490,
#44491,#44492,#44493,#44494,#44495,#44496,#44497,#44498,#44499,#44500,#44501,
#44502,#44503,#44504,#44505,#44506,#44507,#44508,#44509,#44510,#44511,#44512,
#44513,#44514,#44515,#44516,#44517,#44518,#44519,#44520,#44521,#44522,#44523,
#44524,#44525,#44526,#44527,#44528,#44529,#44530,#44531,#44532,#44533,#44534,
#44535,#44536,#44537,#44538,#44539,#44540,#44541,#44542,#44543,#44544,#44545,
#44546,#44547,#44548,#44549,#44550,#44551,#44552,#44553,#44554,#44555,#44556,
#44557,#44558,#44559,#44560,#44561,#44562,#44563,#44564,#44565,#44566,#44567,
#44568,#44569,#44570,#44571,#44572,#44573,#44574,#44575,#44576,#44577,#44578,
#44579,#44580,#44581,#44582,#44583,#44584,#44585,#44586,#44587,#44588,#44589,
#44590,#44591,#44592,#44593,#44594,#44595,#44596,#44597,#44598,#44599,#44600,
#44601,#44602,#44603,#44604,#44605,#44606,#44607,#44608,#44609,#44610,#44611,
#44612,#44613,#44614,#44615,#44616,#44617,#44618,#44619,#44620,#44621,#44622,
#44623,#44624,#44625,#44626,#44627,#44628,#44629,#44630,#44631,#44632,#44633,
#44634),.UNSPECIFIED.,.F.,.F.,(4,3,3,3,3,3,3,3,3,3,3,3,3,3,3,3,3,3,3,3,
3,3,3,3,3,3,3,3,3,3,3,3,3,3,3,3,3,3,3,3,3,3,3,3,3,3,3,3,3,3,3,3,3,3,3,3,
3,3,3,3,3,3,3,3,3,3,3,3,3,3,3,3,3,3,3,4),(72.256631032715,72.3401482880491,
72.4235629091826,72.5068952574145,72.5901656203862,72.6734020156145,72.7566222960338,
72.8398447389392,72.9230876193702,73.0064192735912,73.0897974893735,73.1733051991883,
73.2398505101789,73.3235972428809,73.4072409198967,73.4908016639628,73.5742995259199,
73.6577620264825,73.7412071619747,73.8246529968176,73.9081175920556,73.9916707774774,
74.07526861105,74.1590001739119,74.2388340123781,74.3225807450801,74.4062244220959,
74.4897851661626,74.5732830281197,74.6567455286824,74.7401906641747,74.8236364990176,
74.9071010942556,74.9906542796775,75.0742521132503,75.1579836761122,75.2378175145772,
75.3215642472792,75.4052079242951,75.4887686683616,75.5722665303182,75.6557290308808,
75.739174166373,75.8226200012158,75.9060845964539,75.9896377818757,76.0732356154484,
76.1569671783103,76.2368010167764,76.3205477494783,76.4041914264938,76.4877521705604,
76.5712500325174,76.6547125330799,76.7381576685721,76.8216035034147,76.9050680986528,
76.9886212840747,77.0722191176474,77.1559506805093,77.2357845189756,77.3195312516775,
77.4031749286932,77.4867356727598,77.5702335347166,77.6536960352794,77.7371411707716,
77.8205870056145,77.9040516008525,77.9876047862744,78.0712026198471,78.1549341827089,
78.2347680211747,78.3361959981597,78.438006168876,78.5398163395922),
 .UNSPECIFIED.);
#405=B_SPLINE_CURVE_WITH_KNOTS('',3,(#44636,#44637,#44638,#44639,#44640,
#44641,#44642,#44643,#44644,#44645,#44646,#44647,#44648,#44649,#44650,#44651,
#44652,#44653,#44654,#44655,#44656,#44657,#44658,#44659,#44660,#44661,#44662,
#44663,#44664,#44665,#44666,#44667,#44668,#44669,#44670,#44671,#44672,#44673,
#44674,#44675,#44676,#44677,#44678,#44679,#44680,#44681,#44682,#44683,#44684,
#44685,#44686,#44687,#44688,#44689,#44690,#44691,#44692,#44693,#44694,#44695,
#44696,#44697,#44698,#44699,#44700,#44701,#44702,#44703,#44704,#44705,#44706,
#44707,#44708,#44709,#44710,#44711,#44712,#44713,#44714,#44715,#44716,#44717,
#44718,#44719,#44720,#44721,#44722,#44723,#44724,#44725,#44726,#44727,#44728,
#44729,#44730,#44731,#44732,#44733,#44734,#44735,#44736,#44737,#44738,#44739,
#44740,#44741,#44742,#44743,#44744,#44745,#44746,#44747,#44748,#44749,#44750,
#44751,#44752,#44753,#44754,#44755,#44756,#44757,#44758,#44759,#44760,#44761,
#44762,#44763,#44764,#44765,#44766,#44767,#44768,#44769,#44770,#44771,#44772,
#44773,#44774,#44775,#44776,#44777,#44778,#44779,#44780,#44781,#44782,#44783,
#44784,#44785,#44786,#44787,#44788,#44789,#44790,#44791,#44792,#44793,#44794,
#44795,#44796,#44797,#44798,#44799,#44800,#44801,#44802,#44803,#44804,#44805,
#44806,#44807,#44808,#44809,#44810,#44811,#44812,#44813,#44814,#44815,#44816,
#44817,#44818,#44819,#44820,#44821,#44822,#44823,#44824,#44825,#44826,#44827,
#44828,#44829,#44830,#44831,#44832,#44833,#44834,#44835,#44836,#44837,#44838,
#44839,#44840,#44841,#44842,#44843,#44844,#44845,#44846,#44847,#44848,#44849,
#44850,#44851,#44852,#44853,#44854,#44855,#44856,#44857,#44858,#44859,#44860,
#44861,#44862,#44863,#44864),.UNSPECIFIED.,.F.,.F.,(4,3,3,3,3,3,3,3,3,3,
3,3,3,3,3,3,3,3,3,3,3,3,3,3,3,3,3,3,3,3,3,3,3,3,3,3,3,3,3,3,3,3,3,3,3,3,
3,3,3,3,3,3,3,3,3,3,3,3,3,3,3,3,3,3,3,3,3,3,3,3,3,3,3,3,3,3,4),(65.9734457255818,
66.077168752151,66.1826616383644,66.2469659947847,66.3307127274868,66.4143564045027,
66.4979171485692,66.581415010526,66.6648775110887,66.748322646581,66.831768481424,
66.9152330766622,66.9987862620842,67.0823840956569,67.1661156585188,67.2459494969839,
67.3296962296859,67.4133399067017,67.4969006507683,67.5803985127249,67.6638610132875,
67.7473061487798,67.8307519836227,67.9142165788608,67.9977697642827,68.0813675978553,
68.1650991607172,68.2449329991831,68.3286797318851,68.4123234089009,68.4958841529674,
68.5793820149241,68.6628445154867,68.7462896509789,68.8297354858217,68.9132000810598,
68.9967532664816,69.0803511000543,69.1640826629161,69.2439165013822,69.3276632340842,
69.4113069111,69.4948676551665,69.5783655171233,69.6618280176859,69.7452731531782,
69.8287189880211,69.9121835832592,69.995736768681,70.0793346022537,70.1630661651156,
70.2429000035814,70.3266467362834,70.4102904132992,70.4938511573656,70.5773490193223,
70.6608115198849,70.7442566553772,70.82770249022,70.9111670854581,70.9947202708799,
71.0783181044525,71.1620496673144,71.2418835057806,71.3256302384826,71.4092739154985,
71.4928346595651,71.5763325215219,71.6597950220846,71.7432401575768,71.8266859924197,
71.9101505876577,71.9937037730796,72.0773016066523,72.1610331695142,72.2408670079797,
72.256631032567),.UNSPECIFIED.);
#406=B_SPLINE_CURVE_WITH_KNOTS('',3,(#44866,#44867,#44868,#44869,#44870,
#44871,#44872,#44873,#44874,#44875,#44876,#44877,#44878,#44879,#44880,#44881,
#44882,#44883,#44884,#44885,#44886,#44887,#44888,#44889,#44890,#44891,#44892,
#44893,#44894,#44895,#44896,#44897,#44898,#44899,#44900,#44901,#44902,#44903,
#44904,#44905,#44906,#44907,#44908,#44909,#44910,#44911,#44912,#44913,#44914,
#44915,#44916,#44917,#44918,#44919,#44920,#44921,#44922,#44923,#44924,#44925,
#44926,#44927,#44928,#44929,#44930,#44931,#44932,#44933,#44934,#44935,#44936,
#44937,#44938,#44939,#44940,#44941,#44942,#44943,#44944,#44945,#44946,#44947,
#44948,#44949,#44950,#44951,#44952,#44953,#44954,#44955,#44956,#44957,#44958,
#44959,#44960,#44961,#44962,#44963,#44964,#44965,#44966,#44967,#44968,#44969,
#44970,#44971,#44972,#44973,#44974,#44975,#44976,#44977,#44978,#44979,#44980,
#44981,#44982,#44983,#44984,#44985,#44986,#44987,#44988,#44989,#44990,#44991,
#44992,#44993,#44994,#44995,#44996,#44997,#44998,#44999,#45000,#45001,#45002,
#45003,#45004,#45005,#45006,#45007,#45008,#45009,#45010,#45011,#45012,#45013,
#45014,#45015,#45016,#45017,#45018,#45019,#45020,#45021,#45022,#45023,#45024,
#45025,#45026,#45027,#45028,#45029,#45030,#45031,#45032,#45033,#45034,#45035,
#45036,#45037,#45038,#45039,#45040,#45041,#45042,#45043,#45044,#45045,#45046,
#45047,#45048,#45049,#45050,#45051,#45052,#45053,#45054,#45055,#45056,#45057,
#45058,#45059,#45060,#45061,#45062,#45063,#45064,#45065,#45066,#45067,#45068,
#45069,#45070,#45071,#45072,#45073,#45074,#45075,#45076,#45077,#45078,#45079,
#45080,#45081,#45082,#45083,#45084,#45085,#45086,#45087,#45088,#45089,#45090,
#45091,#45092,#45093,#45094),.UNSPECIFIED.,.F.,.F.,(4,3,3,3,3,3,3,3,3,3,
3,3,3,3,3,3,3,3,3,3,3,3,3,3,3,3,3,3,3,3,3,3,3,3,3,3,3,3,3,3,3,3,3,3,3,3,
3,3,3,3,3,3,3,3,3,3,3,3,3,3,3,3,3,3,3,3,3,3,3,3,3,3,3,3,3,3,4),(59.6902604182078,
59.7757032004822,59.8611946417817,59.946749287853,60.0324436450503,60.1182148552943,
60.2041428744123,60.2530649815898,60.3368117142918,60.4204553913077,60.5040161353741,
60.5875139973306,60.6709764978933,60.7544216333856,60.8378674682284,60.9213320634666,
61.0048852488885,61.0884830824612,61.1722146453231,61.2520484837889,61.3357952164908,
61.4194388935065,61.5029996375732,61.58649749953,61.6699600000926,61.7534051355847,
61.8368509704275,61.9203155656657,62.0038687510876,62.0874665846602,62.1711981475221,
62.2510319859881,62.3347787186901,62.4184223957058,62.5019831397724,62.5854810017289,
62.6689435022915,62.7523886377836,62.8358344726266,62.9192990678649,63.0028522532868,
63.0864500868593,63.1701816497212,63.2500154881873,63.3337622208893,63.4174058979051,
63.5009666419717,63.5844645039286,63.6679270044913,63.7513721399835,63.8348179748266,
63.9182825700649,64.0018357554867,64.0854335890596,64.1691651519215,64.2489989903864,
64.3327457230884,64.4163894001042,64.4999501441702,64.5834480061277,64.6669105066903,
64.7503556421825,64.8338014770253,64.917266072263,65.0008192576848,65.0844170912573,
65.1681486541192,65.2479824925856,65.3309728091399,65.4138315333062,65.4966144831197,
65.5793404606703,65.6620282206894,65.744715102943,65.8273989459123,65.9101328758718,
65.9734457253874),.UNSPECIFIED.);
#407=B_SPLINE_CURVE_WITH_KNOTS('',3,(#45096,#45097,#45098,#45099,#45100,
#45101,#45102,#45103,#45104,#45105,#45106,#45107,#45108,#45109,#45110,#45111,
#45112,#45113,#45114,#45115,#45116,#45117,#45118,#45119,#45120,#45121,#45122,
#45123,#45124,#45125,#45126,#45127,#45128,#45129,#45130,#45131,#45132,#45133,
#45134,#45135,#45136,#45137,#45138,#45139,#45140,#45141,#45142,#45143,#45144,
#45145,#45146,#45147,#45148,#45149,#45150,#45151,#45152,#45153,#45154,#45155,
#45156,#45157,#45158,#45159,#45160,#45161,#45162,#45163,#45164,#45165,#45166,
#45167,#45168,#45169,#45170,#45171,#45172,#45173,#45174,#45175,#45176,#45177,
#45178,#45179,#45180,#45181,#45182,#45183,#45184,#45185,#45186,#45187,#45188,
#45189,#45190,#45191,#45192,#45193,#45194,#45195,#45196,#45197,#45198,#45199,
#45200,#45201,#45202,#45203,#45204,#45205,#45206,#45207,#45208,#45209,#45210,
#45211,#45212,#45213,#45214,#45215,#45216,#45217,#45218,#45219,#45220,#45221,
#45222,#45223,#45224,#45225,#45226,#45227,#45228,#45229,#45230,#45231,#45232,
#45233,#45234,#45235,#45236,#45237,#45238,#45239,#45240,#45241,#45242,#45243,
#45244,#45245,#45246,#45247,#45248,#45249,#45250,#45251,#45252,#45253,#45254,
#45255,#45256,#45257,#45258,#45259,#45260,#45261,#45262,#45263,#45264,#45265,
#45266,#45267,#45268,#45269,#45270,#45271,#45272,#45273,#45274,#45275,#45276,
#45277,#45278,#45279,#45280,#45281,#45282,#45283,#45284,#45285,#45286,#45287,
#45288,#45289,#45290,#45291,#45292,#45293,#45294,#45295,#45296,#45297,#45298,
#45299,#45300,#45301,#45302,#45303,#45304,#45305,#45306,#45307,#45308,#45309,
#45310,#45311,#45312,#45313,#45314,#45315,#45316,#45317,#45318,#45319,#45320,
#45321,#45322,#45323,#45324),.UNSPECIFIED.,.F.,.F.,(4,3,3,3,3,3,3,3,3,3,
3,3,3,3,3,3,3,3,3,3,3,3,3,3,3,3,3,3,3,3,3,3,3,3,3,3,3,3,3,3,3,3,3,3,3,3,
3,3,3,3,3,3,3,3,3,3,3,3,3,3,3,3,3,3,3,3,3,3,3,3,3,3,3,3,3,3,4),(53.4070751111433,
53.4894981066909,53.5718383807227,53.6577540791817,53.7399988815535,53.8222302256025,
53.9044671278617,53.9867286072932,54.0690777661479,54.1514786212285,54.2339950563424,
54.2591639683948,54.3429107010967,54.4265543781124,54.5101151221791,54.5936129841357,
54.6770754846984,54.7605206201908,54.8439664550337,54.9274310502718,55.0109842356937,
55.0945820692664,55.1783136321283,55.2581474705939,55.341894203296,55.4255378803119,
55.5090986243784,55.592596486335,55.6760589868977,55.75950412239,55.8429499572326,
55.9264145524706,56.0099677378925,56.0935655714652,56.177297134327,56.2571309727931,
56.3408777054951,56.4245213825109,56.5080821265771,56.5915799885338,56.6750424890964,
56.7584876245886,56.8419334594315,56.9253980546696,57.0089512400915,57.0925490736641,
57.1762806365259,57.2561144749923,57.3398612076942,57.42350488471,57.5070656287766,
57.5905634907332,57.6740259912958,57.757471126788,57.8409169616306,57.9243815568686,
58.0079347422905,58.0915325758632,58.1752641387251,58.2550979771914,58.3388447098935,
58.4224883869095,58.5060491309762,58.5895469929326,58.6730094934953,58.7564546289875,
58.8399004638304,58.9233650590685,59.0069182444905,59.0905160780629,59.1742476409249,
59.2540814793906,59.3450829724981,59.4357708837664,59.526265849522,59.6164523540533,
59.6902604180762),.UNSPECIFIED.);
#408=B_SPLINE_CURVE_WITH_KNOTS('',3,(#45326,#45327,#45328,#45329,#45330,
#45331,#45332,#45333,#45334,#45335,#45336,#45337,#45338,#45339,#45340,#45341,
#45342,#45343,#45344,#45345,#45346,#45347,#45348,#45349,#45350,#45351,#45352,
#45353,#45354,#45355,#45356,#45357,#45358,#45359,#45360,#45361,#45362,#45363,
#45364,#45365,#45366,#45367,#45368,#45369,#45370,#45371,#45372,#45373,#45374,
#45375,#45376,#45377,#45378,#45379,#45380,#45381,#45382,#45383,#45384,#45385,
#45386,#45387,#45388,#45389,#45390,#45391,#45392,#45393,#45394,#45395,#45396,
#45397,#45398,#45399,#45400,#45401,#45402,#45403,#45404,#45405,#45406,#45407,
#45408,#45409,#45410,#45411,#45412,#45413,#45414,#45415,#45416,#45417,#45418,
#45419,#45420,#45421,#45422,#45423,#45424,#45425,#45426,#45427,#45428,#45429,
#45430,#45431,#45432,#45433,#45434,#45435,#45436,#45437,#45438,#45439,#45440,
#45441,#45442,#45443,#45444,#45445,#45446,#45447,#45448,#45449,#45450,#45451,
#45452,#45453,#45454,#45455,#45456,#45457,#45458,#45459,#45460,#45461,#45462,
#45463,#45464,#45465,#45466,#45467,#45468,#45469,#45470,#45471,#45472,#45473,
#45474,#45475,#45476,#45477,#45478,#45479,#45480,#45481,#45482,#45483,#45484,
#45485,#45486,#45487,#45488,#45489,#45490,#45491,#45492,#45493,#45494,#45495,
#45496,#45497,#45498,#45499,#45500,#45501,#45502,#45503,#45504,#45505,#45506,
#45507,#45508,#45509,#45510,#45511,#45512,#45513,#45514,#45515,#45516,#45517,
#45518,#45519,#45520,#45521,#45522,#45523,#45524,#45525,#45526,#45527,#45528,
#45529,#45530,#45531,#45532,#45533,#45534,#45535,#45536,#45537,#45538,#45539,
#45540,#45541,#45542,#45543,#45544,#45545,#45546,#45547,#45548),
 .UNSPECIFIED.,.F.,.F.,(4,3,3,3,3,3,3,3,3,3,3,3,3,3,3,3,3,3,3,3,3,3,3,3,
3,3,3,3,3,3,3,3,3,3,3,3,3,3,3,3,3,3,3,3,3,3,3,3,3,3,3,3,3,3,3,3,3,3,3,3,
3,3,3,3,3,3,3,3,3,3,3,3,3,3,4),(47.1238898038487,47.2662794530006,47.3500261857027,
47.4336698627184,47.5172306067851,47.6007284687418,47.6841909693046,47.7676361047969,
47.8510819396398,47.9345465348779,48.0180997202998,48.1016975538725,48.1854291167344,
48.2652629551998,48.3490096879018,48.4326533649175,48.5162141089841,48.5997119709408,
48.6831744715034,48.7666196069956,48.8500654418384,48.9335300370765,49.0170832224984,
49.1006810560709,49.1844126189328,49.2642464573989,49.3479931901008,49.4316368671166,
49.5151976111831,49.5986954731397,49.6821579737023,49.7656031091945,49.8490489440373,
49.9325135392754,50.0160667246972,50.0996645582698,50.1833961211316,50.2632299595981,
50.3469766923001,50.4306203693159,50.5141811133825,50.5976789753392,50.6811414759019,
50.7645866113942,50.8480324462371,50.9314970414752,51.0150502268971,51.0986480604698,
51.1823796233317,51.2622134617973,51.3459601944993,51.4296038715151,51.5131646155817,
51.5966624775383,51.6801249781009,51.7635701135932,51.8470159484361,51.9304805436741,
52.014033729096,52.0976315626686,52.1813631255305,52.2611969639964,52.3449436966982,
52.4285873737139,52.5121481177803,52.5956459797368,52.6791084802993,52.7625536157914,
52.845999450634,52.9294640458718,53.0130172312935,53.0966150648661,53.1803466277278,
53.2601804661956,53.4070751110283),.UNSPECIFIED.);
#409=B_SPLINE_CURVE_WITH_KNOTS('',3,(#45550,#45551,#45552,#45553,#45554,
#45555,#45556,#45557,#45558,#45559,#45560,#45561,#45562,#45563,#45564,#45565,
#45566,#45567,#45568,#45569,#45570,#45571,#45572,#45573,#45574,#45575,#45576,
#45577,#45578,#45579,#45580,#45581,#45582,#45583,#45584,#45585,#45586,#45587,
#45588,#45589,#45590,#45591,#45592,#45593,#45594,#45595,#45596,#45597,#45598,
#45599,#45600,#45601,#45602,#45603,#45604,#45605,#45606,#45607,#45608,#45609,
#45610,#45611,#45612,#45613,#45614,#45615,#45616,#45617,#45618,#45619,#45620,
#45621,#45622,#45623,#45624,#45625,#45626,#45627,#45628,#45629,#45630,#45631,
#45632,#45633,#45634,#45635,#45636,#45637,#45638,#45639,#45640,#45641,#45642,
#45643,#45644,#45645,#45646,#45647,#45648,#45649,#45650,#45651,#45652,#45653,
#45654,#45655,#45656,#45657,#45658,#45659,#45660,#45661,#45662,#45663,#45664,
#45665,#45666,#45667,#45668,#45669,#45670,#45671,#45672,#45673,#45674,#45675,
#45676,#45677,#45678,#45679,#45680,#45681,#45682,#45683,#45684,#45685,#45686,
#45687,#45688,#45689,#45690,#45691,#45692,#45693,#45694,#45695,#45696,#45697,
#45698,#45699,#45700,#45701,#45702,#45703,#45704,#45705,#45706,#45707,#45708,
#45709,#45710,#45711,#45712,#45713,#45714,#45715,#45716,#45717,#45718,#45719,
#45720,#45721,#45722,#45723,#45724,#45725,#45726,#45727,#45728,#45729,#45730,
#45731,#45732,#45733,#45734,#45735,#45736,#45737,#45738,#45739,#45740,#45741,
#45742,#45743,#45744,#45745,#45746,#45747,#45748,#45749,#45750,#45751,#45752,
#45753,#45754,#45755,#45756,#45757,#45758,#45759,#45760,#45761,#45762,#45763,
#45764,#45765,#45766,#45767,#45768,#45769,#45770,#45771,#45772,#45773,#45774,
#45775,#45776,#45777,#45778),.UNSPECIFIED.,.F.,.F.,(4,3,3,3,3,3,3,3,3,3,
3,3,3,3,3,3,3,3,3,3,3,3,3,3,3,3,3,3,3,3,3,3,3,3,3,3,3,3,3,3,3,3,3,3,3,3,
3,3,3,3,3,3,3,3,3,3,3,3,3,3,3,3,3,3,3,3,3,3,3,3,3,3,3,3,3,3,4),(40.8407044968042,
40.9310285927585,41.0217286330852,41.1126186716987,41.2038067298644,41.2723784398056,
41.3561251725094,41.4397688495271,41.5233295935954,41.6068274555541,41.6902899561186,
41.7737350916128,41.8571809264576,41.9406455216977,42.0241987071215,42.1077965406961,
42.1915281035599,42.2713619420048,42.355108674706,42.438752351721,42.5223130957869,
42.6058109577429,42.6892734583047,42.7727185937962,42.8561644286382,42.9396290238755,
43.0231822092966,43.1067800428684,43.1905116057295,43.2703454442039,43.3540921769058,
43.4377358539216,43.521296597988,43.6047944599447,43.6882569605072,43.7717020959995,
43.8551479308422,43.9386125260803,44.0221657115021,44.1057635450746,44.1894951079364,
44.2693289464031,44.3530756791053,44.4367193561213,44.5202801001881,44.6037779621451,
44.687240462708,44.7706855982005,44.8541314330436,44.937596028282,45.0211492137041,
45.104747047277,45.1884786101391,45.2683124486023,45.3520591813042,45.4357028583199,
45.5192636023864,45.6027614643429,45.6862239649055,45.7696691003977,45.8531149352404,
45.9365795304784,46.0201327159002,46.1037305494727,46.1874621123345,46.2672959508014,
46.349822107809,46.432245982627,46.5187014602649,46.6009805544563,46.6832282441854,
46.7654635518224,46.8477054867025,46.9300093779677,47.0123494712962,47.0947847624809,
47.1238898037298),.UNSPECIFIED.);
#410=B_SPLINE_CURVE_WITH_KNOTS('',3,(#45780,#45781,#45782,#45783,#45784,
#45785,#45786,#45787,#45788,#45789,#45790,#45791,#45792,#45793,#45794,#45795,
#45796,#45797,#45798,#45799,#45800,#45801,#45802,#45803,#45804,#45805,#45806,
#45807,#45808,#45809,#45810,#45811,#45812,#45813,#45814,#45815,#45816,#45817,
#45818,#45819,#45820,#45821,#45822,#45823,#45824,#45825,#45826,#45827,#45828,
#45829,#45830,#45831,#45832,#45833,#45834,#45835,#45836,#45837,#45838,#45839,
#45840,#45841,#45842,#45843,#45844,#45845,#45846,#45847,#45848,#45849,#45850,
#45851,#45852,#45853,#45854,#45855,#45856,#45857,#45858,#45859,#45860,#45861,
#45862,#45863,#45864,#45865,#45866,#45867,#45868,#45869,#45870,#45871,#45872,
#45873,#45874,#45875,#45876,#45877,#45878,#45879,#45880,#45881,#45882,#45883,
#45884,#45885,#45886,#45887,#45888,#45889,#45890,#45891,#45892,#45893,#45894,
#45895,#45896,#45897,#45898,#45899,#45900,#45901,#45902,#45903,#45904,#45905,
#45906,#45907,#45908,#45909,#45910,#45911,#45912,#45913,#45914,#45915,#45916,
#45917,#45918,#45919,#45920,#45921,#45922,#45923,#45924,#45925,#45926,#45927,
#45928,#45929,#45930,#45931,#45932,#45933,#45934,#45935,#45936,#45937,#45938,
#45939,#45940,#45941,#45942,#45943,#45944,#45945,#45946,#45947,#45948,#45949,
#45950,#45951,#45952,#45953,#45954,#45955,#45956,#45957,#45958,#45959,#45960,
#45961,#45962,#45963,#45964,#45965,#45966,#45967,#45968,#45969,#45970,#45971,
#45972,#45973,#45974,#45975,#45976,#45977,#45978,#45979,#45980,#45981,#45982,
#45983,#45984,#45985,#45986,#45987,#45988,#45989,#45990,#45991,#45992,#45993,
#45994,#45995,#45996,#45997,#45998,#45999,#46000,#46001,#46002,#46003,#46004,
#46005,#46006,#46007,#46008),.UNSPECIFIED.,.F.,.F.,(4,3,3,3,3,3,3,3,3,3,
3,3,3,3,3,3,3,3,3,3,3,3,3,3,3,3,3,3,3,3,3,3,3,3,3,3,3,3,3,3,3,3,3,3,3,3,
3,3,3,3,3,3,3,3,3,3,3,3,3,3,3,3,3,3,3,3,3,3,3,3,3,3,3,3,3,3,4),(34.5575191894895,
34.6402936887573,34.7230330620196,34.8057559307772,34.8884809671239,34.9712268416032,
35.054061493518,35.136943771928,35.2199537508165,35.2784774266106,35.3622241593953,
35.4458678364949,35.5294285806463,35.6129264426885,35.6963889433377,35.7798340789172,
35.8632799138479,35.9467445091739,36.0302976946841,36.1138955283453,36.1976270912952,
36.2774609288098,36.3612076614882,36.4448513384802,36.5284120825231,36.6119099444563,
36.6953724449949,36.7788175804631,36.8622634152818,36.9457280104959,37.0292811958939,
37.1128790294426,37.196610592281,37.276444431009,37.3601911637012,37.4438348407069,
37.5273955847632,37.6108934467099,37.6943559472619,37.7778010827435,37.8612469175754,
37.9447115128023,38.0282646982131,38.1118625317746,38.1955940946252,38.2754279332081,
38.3591746659222,38.4428183429503,38.526379087029,38.6098769489982,38.6933394495735,
38.7767845850787,38.8602304199347,38.9436950151855,39.0272482006204,39.110846034206,
39.194577597081,39.2744114354073,39.358158168105,39.4418018451164,39.5253625891787,
39.6088604511311,39.6923229516894,39.7757680871773,39.8592139220161,39.9426785172497,
40.0262317026673,40.1098295362355,40.1935610990931,40.2733949376064,40.3591926183833,
40.4448691100682,40.5304395102994,40.6158946374186,40.7012820751929,40.7866066094072,
40.8407044966691),.UNSPECIFIED.);
#411=B_SPLINE_CURVE_WITH_KNOTS('',3,(#46010,#46011,#46012,#46013,#46014,
#46015,#46016,#46017,#46018,#46019,#46020,#46021,#46022,#46023,#46024,#46025,
#46026,#46027,#46028,#46029,#46030,#46031,#46032,#46033,#46034,#46035,#46036,
#46037,#46038,#46039,#46040,#46041,#46042,#46043,#46044,#46045,#46046,#46047,
#46048,#46049,#46050,#46051,#46052,#46053,#46054,#46055,#46056,#46057,#46058,
#46059,#46060,#46061,#46062,#46063,#46064,#46065,#46066,#46067,#46068,#46069,
#46070,#46071,#46072,#46073,#46074,#46075,#46076,#46077,#46078,#46079,#46080,
#46081,#46082,#46083,#46084,#46085,#46086,#46087,#46088,#46089,#46090,#46091,
#46092,#46093,#46094,#46095,#46096,#46097,#46098,#46099,#46100,#46101,#46102,
#46103,#46104,#46105,#46106,#46107,#46108,#46109,#46110,#46111,#46112,#46113,
#46114,#46115,#46116,#46117,#46118,#46119,#46120,#46121,#46122,#46123,#46124,
#46125,#46126,#46127,#46128,#46129,#46130,#46131,#46132,#46133,#46134,#46135,
#46136,#46137,#46138,#46139,#46140,#46141,#46142,#46143,#46144,#46145,#46146,
#46147,#46148,#46149,#46150,#46151,#46152,#46153,#46154,#46155,#46156,#46157,
#46158,#46159,#46160,#46161,#46162,#46163,#46164,#46165,#46166,#46167,#46168,
#46169,#46170,#46171,#46172,#46173,#46174,#46175,#46176,#46177,#46178,#46179,
#46180,#46181,#46182,#46183,#46184,#46185,#46186,#46187,#46188,#46189,#46190,
#46191,#46192,#46193,#46194,#46195,#46196,#46197,#46198,#46199,#46200,#46201,
#46202,#46203,#46204,#46205,#46206,#46207,#46208,#46209,#46210,#46211,#46212,
#46213,#46214,#46215,#46216,#46217,#46218,#46219,#46220,#46221,#46222,#46223,
#46224,#46225,#46226,#46227,#46228,#46229,#46230,#46231,#46232,#46233,#46234,
#46235,#46236,#46237,#46238),.UNSPECIFIED.,.F.,.F.,(4,3,3,3,3,3,3,3,3,3,
3,3,3,3,3,3,3,3,3,3,3,3,3,3,3,3,3,3,3,3,3,3,3,3,3,3,3,3,3,3,3,3,3,3,3,3,
3,3,3,3,3,3,3,3,3,3,3,3,3,3,3,3,3,3,3,3,3,3,3,3,3,3,3,3,3,3,4),(28.2743338823098,
28.2855929112165,28.3693396385187,28.4529833100496,28.5365440485524,28.6200419048725,
28.703504399708,28.7869495294187,28.8703953584308,28.9538599477941,29.0374131273048,
29.1210109549371,29.2047425118682,29.2845764134156,29.3683231497121,29.4519668303631,
29.5355275781013,29.6190254437621,29.7024879480652,29.7859330873194,29.8693789259423,
29.952843524975,30.0363967141929,30.1199945515685,30.2037261182066,30.2835599156148,
30.3673066477708,30.4509503242413,30.5345110677637,30.6180089291779,30.7014714292028,
30.7849165641603,30.8683623984718,30.9518269931825,31.0353801780864,31.1189780111453,
31.202709573506,31.282543417814,31.3662901498208,31.4499338261296,31.5334945694783,
31.616992430707,31.7004549305288,31.7839000652725,31.8673458993597,31.9508104938358,
32.0343636784899,32.1179615112904,32.2016930733804,32.2815269200131,32.3652736532667,
32.4489173308407,32.5324780754713,32.6159759379975,32.6994384391356,32.7828835752069,
32.866329410632,32.9497940064547,33.0333471924619,33.1169450266212,33.2006765900661,
33.2805104222123,33.364257154793,33.4479008316872,33.5314615756317,33.614959437466,
33.6984219379065,33.7818670732767,33.8653129079977,33.9487775031143,34.0323306884159,
34.1159285218687,34.1996600846128,34.2794939244115,34.384509295408,34.4879029932419,
34.5575191893829),.UNSPECIFIED.);
#412=B_SPLINE_CURVE_WITH_KNOTS('',3,(#46240,#46241,#46242,#46243,#46244,
#46245,#46246,#46247,#46248,#46249,#46250,#46251,#46252,#46253,#46254,#46255,
#46256,#46257,#46258,#46259,#46260,#46261,#46262,#46263,#46264,#46265,#46266,
#46267,#46268,#46269,#46270,#46271,#46272,#46273,#46274,#46275,#46276,#46277,
#46278,#46279,#46280,#46281,#46282,#46283,#46284,#46285,#46286,#46287,#46288,
#46289,#46290,#46291,#46292,#46293,#46294,#46295,#46296,#46297,#46298,#46299,
#46300,#46301,#46302,#46303,#46304,#46305,#46306,#46307,#46308,#46309,#46310,
#46311,#46312,#46313,#46314,#46315,#46316,#46317,#46318,#46319,#46320,#46321,
#46322,#46323,#46324,#46325,#46326,#46327,#46328,#46329,#46330,#46331,#46332,
#46333,#46334,#46335,#46336,#46337,#46338,#46339,#46340,#46341,#46342,#46343,
#46344,#46345,#46346,#46347,#46348,#46349,#46350,#46351,#46352,#46353,#46354,
#46355,#46356,#46357,#46358,#46359,#46360,#46361,#46362,#46363,#46364,#46365,
#46366,#46367,#46368,#46369,#46370,#46371,#46372,#46373,#46374,#46375,#46376,
#46377,#46378,#46379,#46380,#46381,#46382,#46383,#46384,#46385,#46386,#46387,
#46388,#46389,#46390,#46391,#46392,#46393,#46394,#46395,#46396,#46397,#46398,
#46399,#46400,#46401,#46402,#46403,#46404,#46405,#46406,#46407,#46408,#46409,
#46410,#46411,#46412,#46413,#46414,#46415,#46416,#46417,#46418,#46419,#46420,
#46421,#46422,#46423,#46424,#46425,#46426,#46427,#46428,#46429,#46430,#46431,
#46432,#46433,#46434,#46435,#46436,#46437,#46438,#46439,#46440,#46441,#46442,
#46443,#46444,#46445,#46446,#46447,#46448,#46449,#46450,#46451,#46452,#46453,
#46454,#46455,#46456,#46457,#46458,#46459,#46460,#46461,#46462,#46463,#46464,
#46465),.UNSPECIFIED.,.F.,.F.,(4,3,3,3,3,3,3,3,3,3,3,3,3,3,3,3,3,3,3,3,
3,3,3,3,3,3,3,3,3,3,3,3,3,3,3,3,3,3,3,3,3,3,3,3,3,3,3,3,3,3,3,3,3,3,3,3,
3,3,3,3,3,3,3,3,3,3,3,3,3,3,3,3,3,3,3,4),(21.9911485752772,22.0915967946116,
22.1933535952714,22.2916918980215,22.3754383367532,22.4590817156296,22.5426421577285,
22.6261397142248,22.7096019050848,22.7930467283347,22.8764922486856,22.9599565274714,
23.0435093951123,23.1271069096784,23.2108381546484,23.2906754002206,23.3744222749988,
23.4580660955009,23.5416269843023,23.6251249920827,23.7085876396076,23.7920329227343,
23.875478905744,23.9589436495423,24.0424969833073,24.1260949653393,24.2098266753587,
24.2896589024198,24.3734056361377,24.4570493145306,24.5406100603324,24.62410792438,
24.7075704275707,24.7910155660182,24.874461404142,24.9579260029855,25.0414791925099,
25.1250770304622,25.2088085981372,25.288642404619,25.3723890968892,25.4560327328708,
25.5395934353476,25.6230912552054,25.7065537130417,25.7899988054317,25.8734445968363,
25.9569091483397,26.040462289803,26.1240600792255,26.2077915980539,26.2876259068181,
26.3713726624105,26.4550163625608,26.5385771299799,26.6220750154812,26.7055375397974,
26.7889826991669,26.8724285579882,26.9558931772836,27.0394463867519,27.1230442444029,
27.2067758311547,27.2866094090173,27.3701908686011,27.4536693631837,27.5370651913173,
27.6203985782601,27.7036973121344,27.7869793990543,27.87026305976,27.9535665122895,
28.0369584520835,28.1203962706263,28.2039646002913,28.2743338822021),
 .UNSPECIFIED.);
#413=B_SPLINE_CURVE_WITH_KNOTS('',3,(#46467,#46468,#46469,#46470,#46471,
#46472,#46473,#46474,#46475,#46476,#46477,#46478,#46479,#46480,#46481,#46482,
#46483,#46484,#46485,#46486,#46487,#46488,#46489,#46490,#46491,#46492,#46493,
#46494,#46495,#46496,#46497,#46498,#46499,#46500,#46501,#46502,#46503,#46504,
#46505,#46506,#46507,#46508,#46509,#46510,#46511,#46512,#46513,#46514,#46515,
#46516,#46517,#46518,#46519,#46520,#46521,#46522,#46523,#46524,#46525,#46526,
#46527,#46528,#46529,#46530,#46531,#46532,#46533,#46534,#46535,#46536,#46537,
#46538,#46539,#46540,#46541,#46542,#46543,#46544,#46545,#46546,#46547,#46548,
#46549,#46550,#46551,#46552,#46553,#46554,#46555,#46556,#46557,#46558,#46559,
#46560,#46561,#46562,#46563,#46564,#46565,#46566,#46567,#46568,#46569,#46570,
#46571,#46572,#46573,#46574,#46575,#46576,#46577,#46578,#46579,#46580,#46581,
#46582,#46583,#46584,#46585,#46586,#46587,#46588,#46589,#46590,#46591,#46592,
#46593,#46594,#46595,#46596,#46597,#46598,#46599,#46600,#46601,#46602,#46603,
#46604,#46605,#46606,#46607,#46608,#46609,#46610,#46611,#46612,#46613,#46614,
#46615,#46616,#46617,#46618,#46619,#46620,#46621,#46622,#46623,#46624,#46625,
#46626,#46627,#46628,#46629,#46630,#46631,#46632,#46633,#46634,#46635,#46636,
#46637,#46638,#46639,#46640,#46641,#46642,#46643,#46644,#46645,#46646,#46647,
#46648,#46649,#46650,#46651,#46652,#46653,#46654,#46655,#46656,#46657,#46658,
#46659,#46660,#46661,#46662,#46663,#46664,#46665,#46666,#46667,#46668,#46669,
#46670,#46671,#46672,#46673,#46674,#46675,#46676,#46677,#46678,#46679,#46680,
#46681,#46682,#46683,#46684,#46685,#46686,#46687,#46688,#46689,#46690,#46691,
#46692,#46693,#46694,#46695),.UNSPECIFIED.,.F.,.F.,(4,3,3,3,3,3,3,3,3,3,
3,3,3,3,3,3,3,3,3,3,3,3,3,3,3,3,3,3,3,3,3,3,3,3,3,3,3,3,3,3,3,3,3,3,3,3,
3,3,3,3,3,3,3,3,3,3,3,3,3,3,3,3,3,3,3,3,3,3,3,3,3,3,3,3,3,3,4),(15.7079632679507,
15.7927756596227,15.8776170867123,15.9625034608706,16.0475130802455,16.132586075745,
16.2178171971746,16.2977908848265,16.3815231744717,16.4651522214982,16.5486981652632,
16.6321810729477,16.7156284375635,16.7990583285799,16.8824888246189,16.9659380008729,
17.0494757269557,17.1330580547515,17.2167741886622,17.2967743870256,17.3805260802118,
17.4641747567812,17.5477405338708,17.6312434567916,17.7147110427228,17.7981612776924,
17.8816122212571,17.9650819296005,18.0486402060587,18.1322431266918,18.2159797182806,
18.2957578892248,18.3795058313357,18.4631507479379,18.5467127602997,18.6302119178264,
18.713675751041,18.7971222415942,18.8805694526949,18.9640354441891,19.0475900498296,
19.1311893189108,19.2149223291237,19.294741391424,19.3784860398764,19.462127604408,
19.5456862101661,19.6291819103589,19.7126422210736,19.7960851499237,19.8795287633862,
19.9629911245534,20.0465420683562,20.130137652657,20.2138669758113,20.2937248936231,
20.3774724818822,20.4611170221827,20.5446786362914,20.6281773740904,20.7116407561995,
20.7950867765832,20.8785334988228,20.9619989831243,21.0455530552162,21.1291517755569,
21.2128842163817,21.2927083958223,21.3800134182358,21.4631567532187,21.5462227252512,
21.6292299062174,21.7121968214489,21.7951548997181,21.8781081024208,21.9610957726353,
21.9911485751302),.UNSPECIFIED.);
#414=B_SPLINE_CURVE_WITH_KNOTS('',3,(#46697,#46698,#46699,#46700,#46701,
#46702,#46703,#46704,#46705,#46706,#46707,#46708,#46709,#46710,#46711,#46712,
#46713,#46714,#46715,#46716,#46717,#46718,#46719,#46720,#46721,#46722,#46723,
#46724,#46725,#46726,#46727,#46728,#46729,#46730,#46731,#46732,#46733,#46734,
#46735,#46736,#46737,#46738,#46739,#46740,#46741,#46742,#46743,#46744,#46745,
#46746,#46747,#46748,#46749,#46750,#46751,#46752,#46753,#46754,#46755,#46756,
#46757,#46758,#46759,#46760,#46761,#46762,#46763,#46764,#46765,#46766,#46767,
#46768,#46769,#46770,#46771,#46772,#46773,#46774,#46775,#46776,#46777,#46778,
#46779,#46780,#46781,#46782,#46783,#46784,#46785,#46786,#46787,#46788,#46789,
#46790,#46791,#46792,#46793,#46794,#46795,#46796,#46797,#46798,#46799,#46800,
#46801,#46802,#46803,#46804,#46805,#46806,#46807,#46808,#46809,#46810,#46811,
#46812,#46813,#46814,#46815,#46816,#46817,#46818,#46819,#46820,#46821,#46822,
#46823,#46824,#46825,#46826,#46827,#46828,#46829,#46830,#46831,#46832,#46833,
#46834,#46835,#46836,#46837,#46838,#46839,#46840,#46841,#46842,#46843,#46844,
#46845,#46846,#46847,#46848,#46849,#46850,#46851,#46852,#46853,#46854,#46855,
#46856,#46857,#46858,#46859,#46860,#46861,#46862,#46863,#46864,#46865,#46866,
#46867,#46868,#46869,#46870,#46871,#46872,#46873,#46874,#46875,#46876,#46877,
#46878,#46879,#46880,#46881,#46882,#46883,#46884,#46885,#46886,#46887,#46888,
#46889,#46890,#46891,#46892),.UNSPECIFIED.,.F.,.F.,(4,3,3,3,3,3,3,3,3,3,
3,3,3,3,3,3,3,3,3,3,3,3,3,3,3,3,3,3,3,3,3,3,3,3,3,3,3,3,3,3,3,3,3,3,3,3,
3,3,3,3,3,3,3,3,3,3,3,3,3,3,3,3,3,3,3,4),(10.3765404525762,10.4587521152597,
10.5408614862217,10.6228899520007,10.7078878797294,10.7898262304058,10.8717530949992,
10.9536876277784,11.0356489885776,11.1177007597849,11.1998064288948,11.2820288092828,
11.3028733738307,11.3867642798309,11.4705527050716,11.5542586078086,11.637901875852,
11.7215096228114,11.8050998805076,11.8886905683685,11.9722996021914,12.0559957390186,
12.1397359346823,12.2236074081934,12.3018568760298,12.3857069936252,12.4694559766231,
12.5531238230789,12.6367304615285,12.7203039013286,12.8038612763562,12.8874205458847,
12.9709996665433,13.0546684603941,13.1383826733204,13.2222307644838,13.300840378229,
13.3844892187341,13.4680338034875,13.5514943658934,13.6348910655576,13.7182512639974,
13.8015934160834,13.8849356807694,13.9682962133096,14.0517451381917,14.1352384369971,
14.2188660501523,14.2998238804282,14.3835979510481,14.4672691368914,14.5508575299305,
14.6343831505939,14.7178734767581,14.8013464742856,14.8848201807277,14.9683126302487,
15.0518934838678,15.1355189278689,15.2192777222846,15.2988073826273,15.3913678981619,
15.4835597219632,15.575511367992,15.6670851757684,15.7079632677804),
 .UNSPECIFIED.);
#415=B_SPLINE_CURVE_WITH_KNOTS('',3,(#46896,#46897,#46898,#46899,#46900,
#46901,#46902,#46903,#46904,#46905,#46906,#46907,#46908,#46909,#46910,#46911,
#46912,#46913,#46914,#46915,#46916,#46917,#46918,#46919,#46920,#46921,#46922,
#46923,#46924,#46925,#46926,#46927,#46928,#46929,#46930,#46931,#46932,#46933,
#46934,#46935,#46936,#46937,#46938,#46939,#46940,#46941,#46942,#46943,#46944,
#46945,#46946,#46947,#46948,#46949,#46950,#46951,#46952,#46953,#46954,#46955,
#46956,#46957,#46958,#46959,#46960,#46961,#46962,#46963,#46964,#46965,#46966,
#46967,#46968,#46969,#46970,#46971,#46972,#46973,#46974,#46975,#46976,#46977,
#46978,#46979,#46980,#46981,#46982,#46983,#46984,#46985,#46986,#46987,#46988,
#46989,#46990,#46991,#46992,#46993,#46994,#46995,#46996,#46997,#46998,#46999,
#47000,#47001,#47002,#47003,#47004,#47005,#47006,#47007,#47008,#47009,#47010,
#47011,#47012,#47013,#47014,#47015,#47016,#47017,#47018,#47019,#47020,#47021,
#47022,#47023,#47024,#47025,#47026,#47027,#47028,#47029,#47030,#47031,#47032,
#47033,#47034,#47035,#47036,#47037,#47038,#47039,#47040),.UNSPECIFIED.,
 .F.,.F.,(4,3,3,3,3,3,3,3,3,3,3,3,3,3,3,3,3,3,3,3,3,3,3,3,3,3,3,3,3,3,3,
3,3,3,3,3,3,3,3,3,3,3,3,3,3,3,3,3,4),(11.6154215191127,11.7134108796421,
11.8137864772846,11.9119452646907,12.0134292674513,12.114913270212,12.1986643687573,
12.2824048936106,12.3661873966993,12.4499889517511,12.5338813874082,12.6144050213115,
12.6992193089131,12.7839581468896,12.8686399159733,12.9532829477551,13.0379222058963,
13.1225629256859,13.2072216877147,13.2919150812395,13.3767142872945,13.4615693245244,
13.5465638834944,13.6133885235107,13.6964430640987,13.7793864236487,13.8622394401368,
13.9450228616774,14.0284415071814,14.1111594185092,14.1938739986228,14.2766039053567,
14.360545935445,14.4434061340962,14.5278890799031,14.6123720257099,14.6962629317101,
14.7800513569509,14.8637572596879,14.9474005277315,15.031008274691,15.1145985323872,
15.1981892202482,15.281798254071,15.3654943908983,15.4492345865619,15.5331060600731,
15.611355527909,15.7079632679504),.UNSPECIFIED.);
#416=B_SPLINE_CURVE_WITH_KNOTS('',3,(#47042,#47043,#47044,#47045,#47046,
#47047,#47048,#47049,#47050,#47051,#47052,#47053,#47054,#47055,#47056,#47057,
#47058,#47059,#47060,#47061,#47062,#47063,#47064,#47065,#47066,#47067,#47068,
#47069,#47070,#47071,#47072,#47073,#47074,#47075,#47076,#47077,#47078,#47079,
#47080,#47081,#47082,#47083,#47084,#47085,#47086,#47087,#47088,#47089,#47090,
#47091,#47092,#47093,#47094,#47095,#47096,#47097,#47098,#47099,#47100,#47101,
#47102,#47103,#47104,#47105,#47106,#47107,#47108,#47109,#47110,#47111,#47112,
#47113,#47114,#47115,#47116,#47117,#47118,#47119,#47120,#47121,#47122,#47123,
#47124,#47125,#47126,#47127,#47128,#47129,#47130,#47131,#47132,#47133,#47134,
#47135,#47136,#47137,#47138,#47139,#47140,#47141,#47142,#47143,#47144,#47145,
#47146,#47147,#47148,#47149,#47150,#47151,#47152,#47153,#47154,#47155,#47156,
#47157,#47158,#47159,#47160,#47161,#47162,#47163,#47164,#47165,#47166,#47167,
#47168,#47169,#47170,#47171,#47172,#47173,#47174,#47175,#47176,#47177,#47178,
#47179,#47180,#47181,#47182,#47183,#47184,#47185,#47186,#47187,#47188,#47189,
#47190,#47191,#47192,#47193,#47194,#47195,#47196,#47197,#47198,#47199,#47200,
#47201,#47202,#47203,#47204,#47205,#47206,#47207,#47208,#47209,#47210,#47211,
#47212,#47213,#47214,#47215,#47216,#47217,#47218,#47219,#47220,#47221,#47222,
#47223,#47224,#47225,#47226,#47227,#47228,#47229,#47230,#47231,#47232,#47233,
#47234,#47235,#47236,#47237,#47238,#47239,#47240,#47241,#47242,#47243,#47244,
#47245,#47246,#47247,#47248,#47249,#47250,#47251,#47252,#47253,#47254,#47255,
#47256,#47257,#47258,#47259,#47260,#47261,#47262,#47263,#47264,#47265,#47266,
#47267,#47268,#47269,#47270),.UNSPECIFIED.,.F.,.F.,(4,3,3,3,3,3,3,3,3,3,
3,3,3,3,3,3,3,3,3,3,3,3,3,3,3,3,3,3,3,3,3,3,3,3,3,3,3,3,3,3,3,3,3,3,3,3,
3,3,3,3,3,3,3,3,3,3,3,3,3,3,3,3,3,3,3,3,3,3,3,3,3,3,3,3,3,3,4),(15.7079632680755,
15.7907619926379,15.8734692466063,15.9561059540638,16.0386978979543,16.1212670757871,
16.2038323011308,16.2864123817455,16.3690765141303,16.4517831983492,16.5346204612354,
16.6103390301082,16.6939878706133,16.7775324553667,16.8609930177726,16.9443897174368,
17.0277499158766,17.1110920679627,17.1944343326486,17.2777948651888,17.3612437900709,
17.4447370888762,17.5283647020315,17.6093225323074,17.6930966029273,17.7767677887705,
17.8603561818097,17.9438818024728,18.0273721286368,18.1108451261642,18.1943188326061,
18.2778112821271,18.3613921357462,18.4450175797472,18.5287763741629,18.6083060345065,
18.6920646129743,18.7757203799082,18.8592934438872,18.9428038418974,19.026279164037,
19.1097372932472,19.1931962821169,19.2766741799582,19.3602408292934,19.4438522358629,
19.5275974224496,19.6072895367057,19.6910218263509,19.7746508733775,19.8581968171425,
19.9416797248271,20.0251270894429,20.1085569804594,20.1919874764985,20.2754366527522,
20.3589743788349,20.4425567066307,20.5262728405414,20.6062730389049,20.6900247320912,
20.7736734086611,20.8572391857509,20.940742108672,21.0242096946032,21.1076599295729,
21.1911108731376,21.2745805814815,21.3581388579396,21.4417417785728,21.5254783701617,
21.605256541104,21.7017295495635,21.7954328009705,21.8932906879561,21.9862257175956,
21.9911485749418),.UNSPECIFIED.);
#417=B_SPLINE_CURVE_WITH_KNOTS('',3,(#47272,#47273,#47274,#47275,#47276,
#47277,#47278,#47279,#47280,#47281,#47282,#47283,#47284,#47285,#47286,#47287,
#47288,#47289,#47290,#47291,#47292,#47293,#47294,#47295,#47296,#47297,#47298,
#47299,#47300,#47301,#47302,#47303,#47304,#47305,#47306,#47307,#47308,#47309,
#47310,#47311,#47312,#47313,#47314,#47315,#47316,#47317,#47318,#47319,#47320,
#47321,#47322,#47323,#47324,#47325,#47326,#47327,#47328,#47329,#47330,#47331,
#47332,#47333,#47334,#47335,#47336,#47337,#47338,#47339,#47340,#47341,#47342,
#47343,#47344,#47345,#47346,#47347,#47348,#47349,#47350,#47351,#47352,#47353,
#47354,#47355,#47356,#47357,#47358,#47359,#47360,#47361,#47362,#47363,#47364,
#47365,#47366,#47367,#47368,#47369,#47370,#47371,#47372,#47373,#47374,#47375,
#47376,#47377,#47378,#47379,#47380,#47381,#47382,#47383,#47384,#47385,#47386,
#47387,#47388,#47389,#47390,#47391,#47392,#47393,#47394,#47395,#47396,#47397,
#47398,#47399,#47400,#47401,#47402,#47403,#47404,#47405,#47406,#47407,#47408,
#47409,#47410,#47411,#47412,#47413,#47414,#47415,#47416,#47417,#47418,#47419,
#47420,#47421,#47422,#47423,#47424,#47425,#47426,#47427,#47428,#47429,#47430,
#47431,#47432,#47433,#47434,#47435,#47436,#47437,#47438,#47439,#47440,#47441,
#47442,#47443,#47444,#47445,#47446,#47447,#47448,#47449,#47450,#47451,#47452,
#47453,#47454,#47455,#47456,#47457,#47458,#47459,#47460,#47461,#47462,#47463,
#47464,#47465,#47466,#47467,#47468,#47469,#47470,#47471,#47472,#47473,#47474,
#47475,#47476,#47477,#47478,#47479,#47480,#47481,#47482,#47483,#47484,#47485,
#47486,#47487,#47488,#47489,#47490,#47491,#47492,#47493,#47494,#47495,#47496,
#47497,#47498,#47499,#47500),.UNSPECIFIED.,.F.,.F.,(4,3,3,3,3,3,3,3,3,3,
3,3,3,3,3,3,3,3,3,3,3,3,3,3,3,3,3,3,3,3,3,3,3,3,3,3,3,3,3,3,3,3,3,3,3,3,
3,3,3,3,3,3,3,3,3,3,3,3,3,3,3,3,3,3,3,3,3,3,3,3,3,3,3,3,3,3,4),(21.99114857513,
22.0754397887712,22.1597448263936,22.2440805180614,22.3284637106311,22.4129619403789,
22.4975279040286,22.5822259836788,22.6042400433032,22.6879846917557,22.7716262562874,
22.8551848620454,22.9386805622383,23.0221408729532,23.1055838018032,23.1890274152657,
23.272489776433,23.3560407202358,23.4396363045367,23.523365627691,23.6032235455024,
23.6869711337616,23.7706156740621,23.854177288171,23.9376760259705,24.0211394080798,
24.1045854284634,24.1880321507029,24.2714976350044,24.3550517070964,24.4386504274371,
24.5223828682619,24.6022070477015,24.6859538746302,24.7695976493655,24.8531584945246,
24.9366564608302,25.020119070352,25.1035643175979,25.1870102668931,25.270474979188,
25.3540282851558,25.4376262413643,25.5213579292257,25.6011905499007,25.6849369886324,
25.7685803675088,25.8521408096079,25.935638366104,26.0191005569639,26.1025453802136,
26.1859909005645,26.2694551793504,26.3530080469912,26.4366055615576,26.5203368065275,
26.6001740520998,26.6839209268779,26.7675647473803,26.8511256361815,26.9346236439619,
27.0180862914868,27.1015315746134,27.1849775576231,27.268442301421,27.3519956351859,
27.4355936172179,27.5193253272373,27.599157554299,27.6835545953003,27.7670084084085,
27.8503813813075,27.9336918132199,28.0188523304923,28.102100334802,28.1882171085557,
28.2743338823095),.UNSPECIFIED.);
#418=B_SPLINE_CURVE_WITH_KNOTS('',3,(#47502,#47503,#47504,#47505,#47506,
#47507,#47508,#47509,#47510,#47511,#47512,#47513,#47514,#47515,#47516,#47517,
#47518,#47519,#47520,#47521,#47522,#47523,#47524,#47525,#47526,#47527,#47528,
#47529,#47530,#47531,#47532,#47533,#47534,#47535,#47536,#47537,#47538,#47539,
#47540,#47541,#47542,#47543,#47544,#47545,#47546,#47547,#47548,#47549,#47550,
#47551,#47552,#47553,#47554,#47555,#47556,#47557,#47558,#47559,#47560,#47561,
#47562,#47563,#47564,#47565,#47566,#47567,#47568,#47569,#47570,#47571,#47572,
#47573,#47574,#47575,#47576,#47577,#47578,#47579,#47580,#47581,#47582,#47583,
#47584,#47585,#47586,#47587,#47588,#47589,#47590,#47591,#47592,#47593,#47594,
#47595,#47596,#47597,#47598,#47599,#47600,#47601,#47602,#47603,#47604,#47605,
#47606,#47607,#47608,#47609,#47610,#47611,#47612,#47613,#47614,#47615,#47616,
#47617,#47618,#47619,#47620,#47621,#47622,#47623,#47624,#47625,#47626,#47627,
#47628,#47629,#47630,#47631,#47632,#47633,#47634,#47635,#47636,#47637,#47638,
#47639,#47640,#47641,#47642,#47643,#47644,#47645,#47646,#47647,#47648,#47649,
#47650,#47651,#47652,#47653,#47654,#47655,#47656,#47657,#47658,#47659,#47660,
#47661,#47662,#47663,#47664,#47665,#47666,#47667,#47668,#47669,#47670,#47671,
#47672,#47673,#47674,#47675,#47676,#47677,#47678,#47679,#47680,#47681,#47682,
#47683,#47684,#47685,#47686,#47687,#47688,#47689,#47690,#47691,#47692,#47693,
#47694,#47695,#47696,#47697,#47698,#47699,#47700,#47701,#47702,#47703,#47704,
#47705,#47706,#47707,#47708,#47709,#47710,#47711,#47712,#47713,#47714,#47715,
#47716,#47717,#47718,#47719,#47720,#47721,#47722,#47723,#47724,#47725,#47726,
#47727,#47728,#47729,#47730),.UNSPECIFIED.,.F.,.F.,(4,3,3,3,3,3,3,3,3,3,
3,3,3,3,3,3,3,3,3,3,3,3,3,3,3,3,3,3,3,3,3,3,3,3,3,3,3,3,3,3,3,3,3,3,3,3,
3,3,3,3,3,3,3,3,3,3,3,3,3,3,3,3,3,3,3,3,3,3,3,3,3,3,3,3,3,3,4),(28.2743338824874,
28.3724085420325,28.4711275974312,28.570569651084,28.5981410564982,28.6818877487685,
28.76553138475,28.8490920872268,28.9325899070845,29.016052364921,29.0994974573111,
29.1829432487156,29.2664078002192,29.3499609416825,29.433558731105,29.5172902499334,
29.5971245586973,29.6808713142898,29.7645150144402,29.8480757818592,29.9315736673606,
30.0150361916768,30.0984813510464,30.1819272098678,30.2653918291633,30.3489450386316,
30.4325428962827,30.5162744830346,30.5961080608965,30.679854791818,30.7634984670824,
30.8470592094284,30.9305570696972,31.0140195686282,31.0974647025234,31.1809105358054,
31.2643751295205,31.3479283134885,31.4315261456426,31.5152577071613,31.5950915630957,
31.6788382903979,31.7624819619288,31.8460427004316,31.9295405567519,32.0130030515874,
32.096448181298,32.1798940103101,32.2633585996735,32.3469117791842,32.4305096068163,
32.5142411637475,32.5940750652948,32.6778218015912,32.7614654822422,32.8450262299803,
32.9285240956412,33.0119865999442,33.0954317391984,33.1788775778212,33.2623421768537,
33.3458953660716,33.4294932034471,33.5132247700852,33.593058567494,33.6763378052535,
33.759514298541,33.8426086416793,33.925641352111,34.0086404852872,34.0916242022808,
34.1746109848179,34.2576193132337,34.3407149954989,34.4238586705803,34.5071251979438,
34.55751918934),.UNSPECIFIED.);
#419=B_SPLINE_CURVE_WITH_KNOTS('',3,(#47732,#47733,#47734,#47735,#47736,
#47737,#47738,#47739,#47740,#47741,#47742,#47743,#47744,#47745,#47746,#47747,
#47748,#47749,#47750,#47751,#47752,#47753,#47754,#47755,#47756,#47757,#47758,
#47759,#47760,#47761,#47762,#47763,#47764,#47765,#47766,#47767,#47768,#47769,
#47770,#47771,#47772,#47773,#47774,#47775,#47776,#47777,#47778,#47779,#47780,
#47781,#47782,#47783,#47784,#47785,#47786,#47787,#47788,#47789,#47790,#47791,
#47792,#47793,#47794,#47795,#47796,#47797,#47798,#47799,#47800,#47801,#47802,
#47803,#47804,#47805,#47806,#47807,#47808,#47809,#47810,#47811,#47812,#47813,
#47814,#47815,#47816,#47817,#47818,#47819,#47820,#47821,#47822,#47823,#47824,
#47825,#47826,#47827,#47828,#47829,#47830,#47831,#47832,#47833,#47834,#47835,
#47836,#47837,#47838,#47839,#47840,#47841,#47842,#47843,#47844,#47845,#47846,
#47847,#47848,#47849,#47850,#47851,#47852,#47853,#47854,#47855,#47856,#47857,
#47858,#47859,#47860,#47861,#47862,#47863,#47864,#47865,#47866,#47867,#47868,
#47869,#47870,#47871,#47872,#47873,#47874,#47875,#47876,#47877,#47878,#47879,
#47880,#47881,#47882,#47883,#47884,#47885,#47886,#47887,#47888,#47889,#47890,
#47891,#47892,#47893,#47894,#47895,#47896,#47897,#47898,#47899,#47900,#47901,
#47902,#47903,#47904,#47905,#47906,#47907,#47908,#47909,#47910,#47911,#47912,
#47913,#47914,#47915,#47916,#47917,#47918,#47919,#47920,#47921,#47922,#47923,
#47924,#47925,#47926,#47927,#47928,#47929,#47930,#47931,#47932,#47933,#47934,
#47935,#47936,#47937,#47938,#47939,#47940,#47941,#47942,#47943,#47944,#47945,
#47946,#47947,#47948,#47949,#47950,#47951,#47952,#47953,#47954,#47955,#47956,
#47957,#47958,#47959,#47960),.UNSPECIFIED.,.F.,.F.,(4,3,3,3,3,3,3,3,3,3,
3,3,3,3,3,3,3,3,3,3,3,3,3,3,3,3,3,3,3,3,3,3,3,3,3,3,3,3,3,3,3,3,3,3,3,3,
3,3,3,3,3,3,3,3,3,3,3,3,3,3,3,3,3,3,3,3,3,3,3,3,3,3,3,3,3,3,4),(34.5575191894891,
34.5920420696932,34.6757888017,34.7594324780089,34.8429932213576,34.9264910825864,
35.0099535824083,35.093398717152,35.1768445512393,35.2603091457156,35.3438623303698,
35.4274601631704,35.5111917252604,35.5910255718923,35.6747723051459,35.7584159827199,
35.8419767273506,35.9254745898766,36.0089370910147,36.0923822270861,36.175828062511,
36.2592926583338,36.342845844341,36.4264436785003,36.5101752419451,36.5900090740915,
36.6737558066723,36.7573994835664,36.840960227511,36.9244580893454,37.0079205897859,
37.0913657251563,37.1748115598773,37.258276154994,37.3418293402957,37.4254271737486,
37.5091587364928,37.5889925762907,37.6727393089074,37.7563829858364,37.8399437298146,
37.9234415916816,38.0069040921527,38.0903492275525,38.1737950623018,38.2572596574455,
38.340812842772,38.4244106762487,38.5081422390145,38.5879760784898,38.6717228112747,
38.7553664883743,38.8389272325257,38.922425094568,39.0058875952173,39.0893327307968,
39.1727785657275,39.2562431610538,39.339796346564,39.4233941802252,39.5071257431751,
39.586959580689,39.6707063133674,39.7543499903594,39.8379107344021,39.9214085963348,
40.0048710968733,40.0883162323415,40.1717620671603,40.2552266623743,40.3387798477722,
40.4223776813209,40.5061092441592,40.5859430828882,40.6947718105575,40.8013950654125,
40.8407044965583),.UNSPECIFIED.);
#420=B_SPLINE_CURVE_WITH_KNOTS('',3,(#47962,#47963,#47964,#47965,#47966,
#47967,#47968,#47969,#47970,#47971,#47972,#47973,#47974,#47975,#47976,#47977,
#47978,#47979,#47980,#47981,#47982,#47983,#47984,#47985,#47986,#47987,#47988,
#47989,#47990,#47991,#47992,#47993,#47994,#47995,#47996,#47997,#47998,#47999,
#48000,#48001,#48002,#48003,#48004,#48005,#48006,#48007,#48008,#48009,#48010,
#48011,#48012,#48013,#48014,#48015,#48016,#48017,#48018,#48019,#48020,#48021,
#48022,#48023,#48024,#48025,#48026,#48027,#48028,#48029,#48030,#48031,#48032,
#48033,#48034,#48035,#48036,#48037,#48038,#48039,#48040,#48041,#48042,#48043,
#48044,#48045,#48046,#48047,#48048,#48049,#48050,#48051,#48052,#48053,#48054,
#48055,#48056,#48057,#48058,#48059,#48060,#48061,#48062,#48063,#48064,#48065,
#48066,#48067,#48068,#48069,#48070,#48071,#48072,#48073,#48074,#48075,#48076,
#48077,#48078,#48079,#48080,#48081,#48082,#48083,#48084,#48085,#48086,#48087,
#48088,#48089,#48090,#48091,#48092,#48093,#48094,#48095,#48096,#48097,#48098,
#48099,#48100,#48101,#48102,#48103,#48104,#48105,#48106,#48107,#48108,#48109,
#48110,#48111,#48112,#48113,#48114,#48115,#48116,#48117,#48118,#48119,#48120,
#48121,#48122,#48123,#48124,#48125,#48126,#48127,#48128,#48129,#48130,#48131,
#48132,#48133,#48134,#48135,#48136,#48137,#48138,#48139,#48140,#48141,#48142,
#48143,#48144,#48145,#48146,#48147,#48148,#48149,#48150,#48151,#48152,#48153,
#48154,#48155,#48156,#48157,#48158,#48159,#48160,#48161,#48162,#48163,#48164,
#48165,#48166,#48167,#48168,#48169,#48170,#48171,#48172,#48173,#48174,#48175,
#48176,#48177,#48178,#48179,#48180,#48181,#48182,#48183,#48184,#48185,#48186,
#48187,#48188,#48189,#48190),.UNSPECIFIED.,.F.,.F.,(4,3,3,3,3,3,3,3,3,3,
3,3,3,3,3,3,3,3,3,3,3,3,3,3,3,3,3,3,3,3,3,3,3,3,3,3,3,3,3,3,3,3,3,3,3,3,
3,3,3,3,3,3,3,3,3,3,3,3,3,3,3,3,3,3,3,3,3,3,3,3,3,3,3,3,3,3,4),(40.8407044966687,
40.9233068860812,41.0060093484569,41.0885407393962,41.1710668185745,41.2536064041252,
41.3364364493657,41.4191012667399,41.5020139259136,41.5849265850873,41.6686733178014,
41.7523169948296,41.8358777389084,41.9193756008778,42.0028381014531,42.0862832369582,
42.169729071814,42.253193667065,42.3367468524999,42.4203446860855,42.5040762489604,
42.5839100872865,42.6676568199842,42.7513004969958,42.8348612410579,42.9183591030104,
43.0018216035687,43.0852667390566,43.1687125738951,43.2521771691288,43.3357303545463,
43.4193281881147,43.5030597509723,43.5828935894856,43.6666403221865,43.7502839992013,
43.8338447432672,43.9173426052228,44.0008051057843,44.0842502412753,44.1676960761171,
44.251160671354,44.3347138567746,44.418311690346,44.5020432532065,44.5818770916848,
44.6656238243886,44.7492675014062,44.8328282454744,44.9163261074329,44.9997886079974,
45.0832337434915,45.1666795783362,45.2501441735762,45.3336973589999,45.4172951925746,
45.5010267554384,45.580860593884,45.6646073265853,45.7482510036006,45.831811747666,
45.9153096096219,45.9987721101838,46.0822172456756,46.1656630805174,46.2491276757548,
46.332680861176,46.4162786947479,46.5000102576091,46.5798440960831,46.6663301926089,
46.7526868044835,46.8389274450679,46.9250352854062,47.0110642688329,47.0970105479747,
47.1238898038483),.UNSPECIFIED.);
#421=B_SPLINE_CURVE_WITH_KNOTS('',3,(#48192,#48193,#48194,#48195,#48196,
#48197,#48198,#48199,#48200,#48201,#48202,#48203,#48204,#48205,#48206,#48207,
#48208,#48209,#48210,#48211,#48212,#48213,#48214,#48215,#48216,#48217,#48218,
#48219,#48220,#48221,#48222,#48223,#48224,#48225,#48226,#48227,#48228,#48229,
#48230,#48231,#48232,#48233,#48234,#48235,#48236,#48237,#48238,#48239,#48240,
#48241,#48242,#48243,#48244,#48245,#48246,#48247,#48248,#48249,#48250,#48251,
#48252,#48253,#48254,#48255,#48256,#48257,#48258,#48259,#48260,#48261,#48262,
#48263,#48264,#48265,#48266,#48267,#48268,#48269,#48270,#48271,#48272,#48273,
#48274,#48275,#48276,#48277,#48278,#48279,#48280,#48281,#48282,#48283,#48284,
#48285,#48286,#48287,#48288,#48289,#48290,#48291,#48292,#48293,#48294,#48295,
#48296,#48297,#48298,#48299,#48300,#48301,#48302,#48303,#48304,#48305,#48306,
#48307,#48308,#48309,#48310,#48311,#48312,#48313,#48314,#48315,#48316,#48317,
#48318,#48319,#48320,#48321,#48322,#48323,#48324,#48325,#48326,#48327,#48328,
#48329,#48330,#48331,#48332,#48333,#48334,#48335,#48336,#48337,#48338,#48339,
#48340,#48341,#48342,#48343,#48344,#48345,#48346,#48347,#48348,#48349,#48350,
#48351,#48352,#48353,#48354,#48355,#48356,#48357,#48358,#48359,#48360,#48361,
#48362,#48363,#48364,#48365,#48366,#48367,#48368,#48369,#48370,#48371,#48372,
#48373,#48374,#48375,#48376,#48377,#48378,#48379,#48380,#48381,#48382,#48383,
#48384,#48385,#48386,#48387,#48388,#48389,#48390,#48391,#48392,#48393,#48394,
#48395,#48396,#48397,#48398,#48399,#48400,#48401,#48402,#48403,#48404,#48405,
#48406,#48407,#48408,#48409,#48410,#48411,#48412,#48413,#48414,#48415,#48416,
#48417),.UNSPECIFIED.,.F.,.F.,(4,3,3,3,3,3,3,3,3,3,3,3,3,3,3,3,3,3,3,3,
3,3,3,3,3,3,3,3,3,3,3,3,3,3,3,3,3,3,3,3,3,3,3,3,3,3,3,3,3,3,3,3,3,3,3,3,
3,3,3,3,3,3,3,3,3,3,3,3,3,3,3,3,3,3,3,4),(47.1238898040433,47.2131016067916,
47.3045331046643,47.3942129592113,47.4865202787468,47.5788275982823,47.6625743309846,
47.7462180080007,47.8297787520674,47.9132766140242,47.9967391145871,48.0801842500797,
48.163630084923,48.2470946801614,48.3306478655835,48.4142456991565,48.4979772620187,
48.5778111004815,48.6615578331834,48.7452015101991,48.8287622542655,48.9122601162221,
48.9957226167846,49.0791677522768,49.1626135871195,49.2460781823574,49.3296313677792,
49.4132292013517,49.4969607642135,49.5767946026806,49.6605413353825,49.7441850123983,
49.8277457564647,49.9112436184213,49.9947061189839,50.0781512544761,50.1615970893189,
50.2450616845569,50.3286148699787,50.4122127035513,50.4959442664131,50.5757781048798,
50.6595248375819,50.7431685145977,50.8267292586643,50.9102271206211,50.9936896211838,
51.0771347566761,51.160580591519,51.2440451867572,51.3275983721791,51.4111962057519,
51.4949277686138,51.574761607079,51.658508339781,51.7421520167969,51.8257127608633,
51.9092106228201,51.9926731233827,52.076118258875,52.1595640937179,52.2430286889561,
52.326581874378,52.4101797079507,52.4939112708126,52.5737451092781,52.6562428621318,
52.7386381122537,52.8221927370766,52.9044434497227,52.9866617918347,53.0688668044213,
53.1534188810252,53.2356870725923,53.3213810917146,53.407075110837),
 .UNSPECIFIED.);
#422=B_SPLINE_CURVE_WITH_KNOTS('',3,(#48419,#48420,#48421,#48422,#48423,
#48424,#48425,#48426,#48427,#48428,#48429,#48430,#48431,#48432,#48433,#48434,
#48435,#48436,#48437,#48438,#48439,#48440,#48441,#48442,#48443,#48444,#48445,
#48446,#48447,#48448,#48449,#48450,#48451,#48452,#48453,#48454,#48455,#48456,
#48457,#48458,#48459,#48460,#48461,#48462,#48463,#48464,#48465,#48466,#48467,
#48468,#48469,#48470,#48471,#48472,#48473,#48474,#48475,#48476,#48477,#48478,
#48479,#48480,#48481,#48482,#48483,#48484,#48485,#48486,#48487,#48488,#48489,
#48490,#48491,#48492,#48493,#48494,#48495,#48496,#48497,#48498,#48499,#48500,
#48501,#48502,#48503,#48504,#48505,#48506,#48507,#48508,#48509,#48510,#48511,
#48512,#48513,#48514,#48515,#48516,#48517,#48518,#48519,#48520,#48521,#48522,
#48523,#48524,#48525,#48526,#48527,#48528,#48529,#48530,#48531,#48532,#48533,
#48534,#48535,#48536,#48537,#48538,#48539,#48540,#48541,#48542,#48543,#48544,
#48545,#48546,#48547,#48548,#48549,#48550,#48551,#48552,#48553,#48554,#48555,
#48556,#48557,#48558,#48559,#48560,#48561,#48562,#48563,#48564,#48565,#48566,
#48567,#48568,#48569,#48570,#48571,#48572,#48573,#48574,#48575,#48576,#48577,
#48578,#48579,#48580,#48581,#48582,#48583,#48584,#48585,#48586,#48587,#48588,
#48589,#48590,#48591,#48592,#48593,#48594,#48595,#48596,#48597,#48598,#48599,
#48600,#48601,#48602,#48603,#48604,#48605,#48606,#48607,#48608,#48609,#48610,
#48611,#48612,#48613,#48614,#48615,#48616,#48617,#48618,#48619,#48620,#48621,
#48622,#48623,#48624,#48625,#48626,#48627,#48628,#48629,#48630,#48631,#48632,
#48633,#48634,#48635,#48636,#48637,#48638,#48639,#48640,#48641,#48642,#48643,
#48644),.UNSPECIFIED.,.F.,.F.,(4,3,3,3,3,3,3,3,3,3,3,3,3,3,3,3,3,3,3,3,
3,3,3,3,3,3,3,3,3,3,3,3,3,3,3,3,3,3,3,3,3,3,3,3,3,3,3,3,3,3,3,3,3,3,3,3,
3,3,3,3,3,3,3,3,3,3,3,3,3,3,3,3,3,3,3,4),(53.4070751110279,53.5404486401583,
53.5727286114773,53.6564753441794,53.7401190211952,53.8236797652618,53.9071776272187,
53.9906401277814,54.0740852632737,54.1575310981167,54.2409956933549,54.3245488787768,
54.4081467123496,54.4918782752115,54.5717121136765,54.6554588463785,54.7391025233943,
54.8226632674608,54.9061611294176,54.9896236299802,55.0730687654725,55.1565146003153,
55.2399791955534,55.3235323809753,55.4071302145479,55.4908617774098,55.5706956158756,
55.6544423485775,55.7380860255933,55.8216467696598,55.9051446316165,55.9886071321791,
56.0720522676713,56.1554981025141,56.2389626977521,56.3225158831739,56.4061137167465,
56.4898452796084,56.5696791180748,56.6534258507768,56.7370695277926,56.8206302718592,
56.9041281338159,56.9875906343785,57.0710357698708,57.1544816047136,57.2379461999517,
57.3214993853736,57.4050972189462,57.4888287818081,57.5686626202739,57.6524093529759,
57.7360530299917,57.8196137740582,57.9031116360149,57.9865741365775,58.0700192720698,
58.1534651069126,58.2369297021506,58.3204828875725,58.4040807211451,58.487812284007,
58.5676461224731,58.6513928551751,58.7350365321909,58.8185972762574,58.9020951382142,
58.9855576387768,59.069002774269,59.1524486091118,59.2359132043498,59.3194663897717,
59.4030642233443,59.4867957862062,59.5666296246723,59.6902604182075),
 .UNSPECIFIED.);
#423=B_SPLINE_CURVE_WITH_KNOTS('',3,(#48646,#48647,#48648,#48649,#48650,
#48651,#48652,#48653,#48654,#48655,#48656,#48657,#48658,#48659,#48660,#48661,
#48662,#48663,#48664,#48665,#48666,#48667,#48668,#48669,#48670,#48671,#48672,
#48673,#48674,#48675,#48676,#48677,#48678,#48679,#48680,#48681,#48682,#48683,
#48684,#48685,#48686,#48687,#48688,#48689,#48690,#48691,#48692,#48693,#48694,
#48695,#48696,#48697,#48698,#48699,#48700,#48701,#48702,#48703,#48704,#48705,
#48706,#48707,#48708,#48709,#48710,#48711,#48712,#48713,#48714,#48715,#48716,
#48717,#48718,#48719,#48720,#48721,#48722,#48723,#48724,#48725,#48726,#48727,
#48728,#48729,#48730,#48731,#48732,#48733,#48734,#48735,#48736,#48737,#48738,
#48739,#48740,#48741,#48742,#48743,#48744,#48745,#48746,#48747,#48748,#48749,
#48750,#48751,#48752,#48753,#48754,#48755,#48756,#48757,#48758,#48759,#48760,
#48761,#48762,#48763,#48764,#48765,#48766,#48767,#48768,#48769,#48770,#48771,
#48772,#48773,#48774,#48775,#48776,#48777,#48778,#48779,#48780,#48781,#48782,
#48783,#48784,#48785,#48786,#48787,#48788,#48789,#48790,#48791,#48792,#48793,
#48794,#48795,#48796,#48797,#48798,#48799,#48800,#48801,#48802,#48803,#48804,
#48805,#48806,#48807,#48808,#48809,#48810,#48811,#48812,#48813,#48814,#48815,
#48816,#48817,#48818,#48819,#48820,#48821,#48822,#48823,#48824,#48825,#48826,
#48827,#48828,#48829,#48830,#48831,#48832,#48833,#48834,#48835,#48836,#48837,
#48838,#48839,#48840,#48841,#48842,#48843,#48844,#48845,#48846,#48847,#48848,
#48849,#48850,#48851,#48852,#48853,#48854,#48855,#48856,#48857,#48858,#48859,
#48860,#48861,#48862,#48863,#48864,#48865,#48866,#48867,#48868,#48869,#48870,
#48871,#48872,#48873,#48874),.UNSPECIFIED.,.F.,.F.,(4,3,3,3,3,3,3,3,3,3,
3,3,3,3,3,3,3,3,3,3,3,3,3,3,3,3,3,3,3,3,3,3,3,3,3,3,3,3,3,3,3,3,3,3,3,3,
3,3,3,3,3,3,3,3,3,3,3,3,3,3,3,3,3,3,3,3,3,3,3,3,3,3,3,3,3,3,4),(59.6902604183383,
59.7727730645136,59.8551978339046,59.937555829786,60.0198741998651,60.1021735226374,
60.1844727762721,60.2667909365586,60.3491942539214,60.4316440876682,60.514216687236,
60.5656131268714,60.6493598595734,60.7330035365893,60.8165642806556,60.9000621426123,
60.9835246431749,61.0669697786671,61.1504156135099,61.2338802087482,61.31743339417,
61.4010312277426,61.4847627906044,61.5645966290706,61.6483433617727,61.7319870387886,
61.8155477828553,61.8990456448121,61.9825081453748,62.0659532808671,62.1493991157099,
62.232863710948,62.3164168963699,62.4000147299426,62.4837462928045,62.5635801312698,
62.6473268639717,62.7309705409874,62.8145312850538,62.8980291470104,62.981491647573,
63.0649367830651,63.148382617908,63.231847213146,63.3154003985678,63.3989982321403,
63.4827297950021,63.5625636334689,63.6463103661709,63.7299540431867,63.8135147872533,
63.89701264921,63.9804751497727,64.063920285265,64.147366120108,64.2308307153459,
64.3143839007678,64.3979817343406,64.4817132972025,64.5615471356681,64.6452938683701,
64.7289375453863,64.8124982894526,64.8959961514093,64.9794586519718,65.0629037874642,
65.1463496223072,65.2298142175456,65.3133674029674,65.39696523654,65.4806967994018,
65.5605306378673,65.652882329379,65.7448720149147,65.8366278894589,65.9280144118952,
65.9734457252248),.UNSPECIFIED.);
#424=B_SPLINE_CURVE_WITH_KNOTS('',3,(#48876,#48877,#48878,#48879,#48880,
#48881,#48882,#48883,#48884,#48885,#48886,#48887,#48888,#48889,#48890,#48891,
#48892,#48893,#48894,#48895,#48896,#48897,#48898,#48899,#48900,#48901,#48902,
#48903,#48904,#48905,#48906,#48907,#48908,#48909,#48910,#48911,#48912,#48913,
#48914,#48915,#48916,#48917,#48918,#48919,#48920,#48921,#48922,#48923,#48924,
#48925,#48926,#48927,#48928,#48929,#48930,#48931,#48932,#48933,#48934,#48935,
#48936,#48937,#48938,#48939,#48940,#48941,#48942,#48943,#48944,#48945,#48946,
#48947,#48948,#48949,#48950,#48951,#48952,#48953,#48954,#48955,#48956,#48957,
#48958,#48959,#48960,#48961,#48962,#48963,#48964,#48965,#48966,#48967,#48968,
#48969,#48970,#48971,#48972,#48973,#48974,#48975,#48976,#48977,#48978,#48979,
#48980,#48981,#48982,#48983,#48984,#48985,#48986,#48987,#48988,#48989,#48990,
#48991,#48992,#48993,#48994,#48995,#48996,#48997,#48998,#48999,#49000,#49001,
#49002,#49003,#49004,#49005,#49006,#49007,#49008,#49009,#49010,#49011,#49012,
#49013,#49014,#49015,#49016,#49017,#49018,#49019,#49020,#49021,#49022,#49023,
#49024,#49025,#49026,#49027,#49028,#49029,#49030,#49031,#49032,#49033,#49034,
#49035,#49036,#49037,#49038,#49039,#49040,#49041,#49042,#49043,#49044,#49045,
#49046,#49047,#49048,#49049,#49050,#49051,#49052,#49053,#49054,#49055,#49056,
#49057,#49058,#49059,#49060,#49061,#49062,#49063,#49064,#49065,#49066,#49067,
#49068,#49069,#49070,#49071,#49072,#49073,#49074,#49075,#49076,#49077,#49078,
#49079,#49080,#49081,#49082,#49083,#49084,#49085,#49086,#49087,#49088,#49089,
#49090,#49091,#49092,#49093,#49094,#49095,#49096,#49097,#49098,#49099,#49100,
#49101,#49102,#49103,#49104),.UNSPECIFIED.,.F.,.F.,(4,3,3,3,3,3,3,3,3,3,
3,3,3,3,3,3,3,3,3,3,3,3,3,3,3,3,3,3,3,3,3,3,3,3,3,3,3,3,3,3,3,3,3,3,3,3,
3,3,3,3,3,3,3,3,3,3,3,3,3,3,3,3,3,3,3,3,3,3,3,3,3,3,3,3,3,3,4),(65.9734457253871,
66.0583137750458,66.1432129355834,66.2281590044431,66.3132300065901,66.3983658996381,
66.4836594664784,66.5595141400664,66.6432608727684,66.7269045497842,66.8104652938508,
66.8939631558075,66.9774256563701,67.0608707918624,67.1443166267054,67.2277812219434,
67.3113344073653,67.3949322409378,67.4786638037997,67.5584976422656,67.6422443749675,
67.7258880519833,67.8094487960498,67.8929466580062,67.9764091585687,68.059854294061,
68.1433001289038,68.2267647241418,68.3103179095636,68.3939157431361,68.477647305998,
68.5574811444648,68.6412278771669,68.7248715541827,68.8084322982493,68.8919301602061,
68.9753926607689,69.0588377962614,69.1422836311044,69.2257482263426,69.3093014117645,
69.3928992453372,69.4766308081992,69.5564646466639,69.6402113793658,69.7238550563815,
69.8074158004482,69.8909136624047,69.9743761629672,70.0578212984594,70.141267133302,
70.22473172854,70.3082849139618,70.3918827475344,70.4756143103962,70.5554481488631,
70.6391948815652,70.722838558581,70.8063993026476,70.8898971646042,70.9733596651668,
71.0568048006591,71.1402506355021,71.2237152307402,71.3072684161621,71.3908662497347,
71.4745978125967,71.5544316510623,71.637669438077,71.7207727177989,71.8037981191682,
71.8867642534451,71.9696896846727,72.0526066766501,72.1355184100973,72.2184668296268,
72.2566310325666),.UNSPECIFIED.);
#425=B_SPLINE_CURVE_WITH_KNOTS('',3,(#49106,#49107,#49108,#49109,#49110,
#49111,#49112,#49113,#49114,#49115,#49116,#49117,#49118,#49119,#49120,#49121,
#49122,#49123,#49124,#49125,#49126,#49127,#49128,#49129,#49130,#49131,#49132,
#49133,#49134,#49135,#49136,#49137,#49138,#49139,#49140,#49141,#49142,#49143,
#49144,#49145,#49146,#49147,#49148,#49149,#49150,#49151,#49152,#49153,#49154,
#49155,#49156,#49157,#49158,#49159,#49160,#49161,#49162,#49163,#49164,#49165,
#49166,#49167,#49168,#49169,#49170,#49171,#49172,#49173,#49174,#49175,#49176,
#49177,#49178,#49179,#49180,#49181,#49182,#49183,#49184,#49185,#49186,#49187,
#49188,#49189,#49190,#49191,#49192,#49193,#49194,#49195,#49196,#49197,#49198,
#49199,#49200,#49201,#49202,#49203,#49204,#49205,#49206,#49207,#49208,#49209,
#49210,#49211,#49212,#49213,#49214,#49215,#49216,#49217,#49218,#49219,#49220,
#49221,#49222,#49223,#49224,#49225,#49226,#49227,#49228,#49229,#49230,#49231,
#49232,#49233,#49234,#49235,#49236,#49237,#49238,#49239,#49240,#49241,#49242,
#49243,#49244,#49245,#49246,#49247,#49248,#49249,#49250,#49251,#49252,#49253,
#49254,#49255,#49256,#49257,#49258,#49259,#49260,#49261,#49262,#49263,#49264,
#49265,#49266,#49267,#49268,#49269,#49270,#49271,#49272,#49273,#49274,#49275,
#49276,#49277,#49278,#49279,#49280,#49281,#49282,#49283,#49284,#49285,#49286,
#49287,#49288,#49289,#49290,#49291,#49292,#49293,#49294,#49295,#49296,#49297,
#49298,#49299,#49300,#49301,#49302,#49303,#49304,#49305,#49306,#49307,#49308,
#49309,#49310,#49311,#49312,#49313,#49314,#49315,#49316,#49317,#49318,#49319,
#49320,#49321,#49322,#49323,#49324,#49325,#49326,#49327,#49328,#49329,#49330,
#49331),.UNSPECIFIED.,.F.,.F.,(4,3,3,3,3,3,3,3,3,3,3,3,3,3,3,3,3,3,3,3,
3,3,3,3,3,3,3,3,3,3,3,3,3,3,3,3,3,3,3,3,3,3,3,3,3,3,3,3,3,3,3,3,3,3,3,3,
3,3,3,3,3,3,3,3,3,3,3,3,3,3,3,3,3,3,3,4),(72.256631032708,72.3574966325378,
72.4597233926165,72.5534151532614,72.6371618859633,72.720805562979,72.8043663070453,
72.8878641690021,72.9713266695647,73.0547718050569,73.1382176398997,73.2216822351377,
73.3052354205595,73.388833254132,73.4725648169938,73.5523986554606,73.6361453881625,
73.7197890651783,73.8033498092448,73.8868476712015,73.9703101717641,74.0537553072564,
74.1372011420992,74.2206657373373,74.3042189227592,74.3878167563318,74.4715483191936,
74.5513821576597,74.6351288903617,74.7187725673775,74.8023333114441,74.8858311734007,
74.9692936739634,75.0527388094557,75.1361846442986,75.2196492395367,75.3032024249585,
75.3868002585312,75.4705318213931,75.5503656598589,75.6341123925609,75.7177560695767,
75.8013168136432,75.8848146755999,75.9682771761625,76.0517223116548,76.1351681464976,
76.2186327417357,76.3021859271575,76.3857837607301,76.469515323592,76.5493491620581,
76.6330958947601,76.7167395717759,76.8003003158424,76.8837981777991,76.9672606783617,
77.050705813854,77.1341516486968,77.2176162439349,77.3011694293568,77.3847672629294,
77.4684988257913,77.5483326642572,77.6319679059608,77.7155001505879,77.7989496406175,
77.8823365457303,77.9656885756253,78.0490237282131,78.132360174458,78.2157160824001,
78.2991605475987,78.382650497063,78.466272073614,78.5398163396007),
 .UNSPECIFIED.);
#426=B_SPLINE_CURVE_WITH_KNOTS('',3,(#49333,#49334,#49335,#49336,#49337,
#49338,#49339,#49340,#49341,#49342,#49343,#49344,#49345,#49346,#49347,#49348,
#49349,#49350,#49351,#49352,#49353,#49354,#49355,#49356,#49357,#49358,#49359,
#49360,#49361,#49362,#49363,#49364,#49365,#49366,#49367,#49368,#49369,#49370,
#49371,#49372,#49373,#49374,#49375,#49376,#49377,#49378,#49379,#49380,#49381,
#49382,#49383,#49384,#49385,#49386,#49387,#49388,#49389,#49390,#49391,#49392,
#49393,#49394,#49395,#49396,#49397,#49398,#49399,#49400,#49401,#49402,#49403,
#49404,#49405,#49406,#49407,#49408,#49409,#49410,#49411,#49412,#49413,#49414,
#49415,#49416,#49417,#49418,#49419,#49420,#49421,#49422,#49423,#49424,#49425,
#49426,#49427,#49428,#49429,#49430,#49431,#49432,#49433,#49434,#49435,#49436,
#49437,#49438,#49439,#49440,#49441,#49442,#49443,#49444,#49445,#49446,#49447,
#49448,#49449,#49450,#49451,#49452,#49453,#49454,#49455,#49456,#49457,#49458,
#49459,#49460,#49461,#49462,#49463,#49464,#49465,#49466,#49467,#49468,#49469,
#49470,#49471,#49472,#49473,#49474,#49475,#49476,#49477,#49478,#49479,#49480,
#49481,#49482,#49483,#49484,#49485,#49486,#49487,#49488,#49489,#49490,#49491,
#49492,#49493,#49494,#49495,#49496,#49497,#49498,#49499,#49500,#49501,#49502,
#49503,#49504,#49505,#49506,#49507,#49508,#49509,#49510,#49511,#49512,#49513,
#49514,#49515,#49516,#49517,#49518,#49519,#49520,#49521,#49522,#49523,#49524,
#49525,#49526,#49527,#49528,#49529,#49530,#49531,#49532,#49533,#49534,#49535,
#49536,#49537,#49538,#49539,#49540,#49541,#49542,#49543,#49544,#49545,#49546,
#49547,#49548,#49549,#49550,#49551,#49552,#49553,#49554,#49555,#49556,#49557,
#49558,#49559,#49560,#49561),.UNSPECIFIED.,.F.,.F.,(4,3,3,3,3,3,3,3,3,3,
3,3,3,3,3,3,3,3,3,3,3,3,3,3,3,3,3,3,3,3,3,3,3,3,3,3,3,3,3,3,3,3,3,3,3,3,
3,3,3,3,3,3,3,3,3,3,3,3,3,3,3,3,3,3,3,3,3,3,3,3,3,3,3,3,3,3,4),(78.5398163397462,
78.5473161664564,78.6310628991584,78.7147065761743,78.7982673202406,78.8817651821975,
78.9652276827602,79.0486728182524,79.1321186530954,79.2155832483335,79.2991364337554,
79.3827342673281,79.46646583019,79.5462996686556,79.6300464013575,79.7136900783733,
79.7972508224399,79.8807486843966,79.9642111849592,80.0476563204514,80.1311021552943,
80.2145667505323,80.2981199359542,80.3817177695268,80.4654493323886,80.5452831708547,
80.6290299035567,80.7126735805725,80.796234324639,80.8797321865956,80.9631946871582,
81.0466398226505,81.1300856574933,81.2135502527314,81.2971034381532,81.3807012717259,
81.4644328345877,81.5442666730539,81.6280134057559,81.7116570827717,81.7952178268383,
81.878715688795,81.9621781893576,82.04562332485,82.1290691596928,82.2125337549309,
82.2960869403528,82.3796847739254,82.4634163367873,82.5432501752531,82.6269969079551,
82.7106405849708,82.7942013290373,82.877699190994,82.9611616915566,83.0446068270489,
83.1280526618917,83.2115172571298,83.2950704425516,83.3786682761242,83.4623998389861,
83.5422336774522,83.6259804101541,83.7096240871698,83.7931848312362,83.8766826931929,
83.9601451937554,84.0435903292477,84.1270361640904,84.2105007593285,84.2940539447503,
84.3776517783229,84.4613833411848,84.5412171796514,84.645685853533,84.748605073981,
84.8230016469258),.UNSPECIFIED.);
#427=B_SPLINE_CURVE_WITH_KNOTS('',3,(#49563,#49564,#49565,#49566,#49567,
#49568,#49569,#49570,#49571,#49572),.UNSPECIFIED.,.F.,.F.,(4,1,1,1,1,1,
1,4),(84.8230016469258,85.5402006818506,86.5391841840497,87.5381676862489,
88.5371511884481,89.5361346906472,90.5351181928464,91.1061869541054),
 .UNSPECIFIED.);
#428=B_SPLINE_CURVE_WITH_KNOTS('',3,(#49574,#49575,#49576,#49577,#49578,
#49579,#49580,#49581,#49582,#49583,#49584,#49585,#49586,#49587,#49588,#49589,
#49590,#49591,#49592,#49593,#49594,#49595,#49596,#49597,#49598,#49599,#49600,
#49601,#49602,#49603,#49604,#49605,#49606,#49607,#49608,#49609,#49610,#49611,
#49612,#49613,#49614,#49615,#49616,#49617,#49618,#49619,#49620,#49621,#49622,
#49623,#49624,#49625,#49626,#49627,#49628,#49629,#49630,#49631,#49632,#49633,
#49634,#49635,#49636,#49637,#49638,#49639,#49640,#49641,#49642,#49643,#49644,
#49645,#49646,#49647,#49648,#49649,#49650,#49651,#49652,#49653,#49654,#49655,
#49656,#49657,#49658,#49659,#49660,#49661,#49662,#49663,#49664,#49665,#49666,
#49667,#49668,#49669,#49670,#49671,#49672,#49673,#49674,#49675,#49676,#49677,
#49678,#49679,#49680,#49681,#49682,#49683,#49684,#49685,#49686,#49687,#49688,
#49689,#49690,#49691,#49692,#49693,#49694,#49695,#49696,#49697,#49698,#49699,
#49700,#49701,#49702,#49703,#49704,#49705,#49706,#49707,#49708,#49709,#49710,
#49711,#49712,#49713,#49714,#49715,#49716,#49717,#49718,#49719,#49720,#49721,
#49722,#49723,#49724,#49725,#49726,#49727,#49728,#49729,#49730,#49731,#49732,
#49733,#49734,#49735,#49736,#49737,#49738,#49739,#49740,#49741,#49742,#49743,
#49744,#49745,#49746,#49747,#49748,#49749,#49750,#49751,#49752,#49753,#49754,
#49755,#49756,#49757,#49758,#49759,#49760,#49761,#49762,#49763,#49764,#49765,
#49766,#49767,#49768,#49769,#49770,#49771,#49772,#49773,#49774,#49775,#49776,
#49777,#49778,#49779,#49780,#49781,#49782,#49783,#49784,#49785,#49786,#49787,
#49788,#49789,#49790,#49791,#49792,#49793,#49794,#49795,#49796,#49797,#49798,
#49799,#49800,#49801,#49802),.UNSPECIFIED.,.F.,.F.,(4,3,3,3,3,3,3,3,3,3,
3,3,3,3,3,3,3,3,3,3,3,3,3,3,3,3,3,3,3,3,3,3,3,3,3,3,3,3,3,3,3,3,3,3,3,3,
3,3,3,3,3,3,3,3,3,3,3,3,3,3,3,3,3,3,3,3,3,3,3,3,3,3,3,3,3,3,4),(91.1061869541054,
91.1967032367233,91.2876073527091,91.3787081395492,91.4701107400683,91.5341016950455,
91.6178484277474,91.7014921047632,91.7850528488296,91.8685507107865,91.9520132113491,
92.0354583468413,92.118904181684,92.2023687769221,92.2859219623439,92.3695197959165,
92.4532513587783,92.5330851972447,92.6168319299467,92.7004756069625,92.7840363510291,
92.8675342129859,92.9509967135485,93.0344418490408,93.1178876838837,93.2013522791218,
93.2849054645438,93.3685032981164,93.4522348609783,93.5320686994439,93.6158154321458,
93.6994591091615,93.783019853228,93.8665177151846,93.9499802157471,94.0334253512393,
94.1168711860821,94.2003357813201,94.2838889667419,94.3674868003145,94.4512183631763,
94.531052201643,94.614798934345,94.6984426113609,94.7820033554274,94.8655012173841,
94.9489637179468,95.0324088534391,95.115854688282,95.1993192835201,95.282872468942,
95.3664703025147,95.4502018653766,95.5300357038422,95.6137824365442,95.6974261135601,
95.7809868576267,95.8644847195834,95.947947220146,96.0313923556383,96.1148381904812,
96.1983027857192,96.2818559711412,96.3654538047138,96.4491853675757,96.5290192060414,
96.6115543549841,96.6939872426548,96.7763390732232,96.858629393003,96.9408873830372,
97.0231320612446,97.1053824317881,97.187694931784,97.2700427524997,97.3524884132919,
97.3893722611632),.UNSPECIFIED.);
#429=B_SPLINE_CURVE_WITH_KNOTS('',3,(#49804,#49805,#49806,#49807,#49808,
#49809,#49810,#49811,#49812,#49813,#49814,#49815,#49816,#49817,#49818,#49819,
#49820,#49821,#49822,#49823,#49824,#49825,#49826,#49827,#49828,#49829,#49830,
#49831,#49832,#49833,#49834,#49835,#49836,#49837,#49838,#49839,#49840,#49841,
#49842,#49843,#49844,#49845,#49846,#49847,#49848,#49849,#49850,#49851,#49852,
#49853,#49854,#49855,#49856,#49857,#49858,#49859,#49860,#49861,#49862,#49863,
#49864,#49865,#49866,#49867,#49868,#49869,#49870,#49871,#49872,#49873,#49874,
#49875,#49876,#49877,#49878,#49879,#49880,#49881,#49882,#49883,#49884,#49885,
#49886,#49887,#49888,#49889,#49890,#49891,#49892,#49893,#49894,#49895,#49896,
#49897,#49898,#49899,#49900,#49901,#49902,#49903,#49904,#49905,#49906,#49907,
#49908,#49909,#49910,#49911,#49912,#49913,#49914,#49915,#49916,#49917,#49918,
#49919,#49920,#49921,#49922,#49923,#49924,#49925,#49926,#49927,#49928,#49929,
#49930,#49931,#49932,#49933,#49934,#49935,#49936,#49937,#49938,#49939,#49940,
#49941,#49942,#49943,#49944,#49945,#49946,#49947,#49948,#49949,#49950,#49951,
#49952,#49953,#49954,#49955,#49956,#49957,#49958,#49959,#49960,#49961,#49962,
#49963,#49964,#49965,#49966,#49967,#49968,#49969,#49970,#49971,#49972,#49973,
#49974,#49975,#49976,#49977,#49978,#49979,#49980,#49981,#49982,#49983,#49984,
#49985,#49986,#49987,#49988,#49989,#49990,#49991,#49992,#49993,#49994,#49995,
#49996,#49997,#49998,#49999,#50000,#50001,#50002,#50003,#50004,#50005,#50006,
#50007,#50008,#50009,#50010,#50011,#50012,#50013,#50014,#50015,#50016,#50017,
#50018,#50019,#50020,#50021,#50022,#50023,#50024,#50025,#50026,#50027,#50028,
#50029),.UNSPECIFIED.,.F.,.F.,(4,3,3,3,3,3,3,3,3,3,3,3,3,3,3,3,3,3,3,3,
3,3,3,3,3,3,3,3,3,3,3,3,3,3,3,3,3,3,3,3,3,3,3,3,3,3,3,3,3,3,3,3,3,3,3,3,
3,3,3,3,3,3,3,3,3,3,3,3,3,3,3,3,3,3,3,4),(97.389372261285,97.5280027082405,
97.6117494409424,97.6953931179581,97.7789538620244,97.8624517239809,97.9459142245435,
98.0293593600356,98.1128051948784,98.1962697901164,98.2798229755382,98.3634208091107,
98.4471523719725,98.5269862104397,98.6107329431417,98.6943766201574,98.777937364224,
98.8614352261807,98.9448977267433,99.0283428622356,99.1117886970785,99.1952532923166,
99.2788064777384,99.3624043113111,99.4461358741729,99.5259697126389,99.6097164453409,
99.6933601223567,99.7769208664232,99.86041872838,99.9438812289426,100.027326364435,
100.110772199278,100.194236794516,100.277789979938,100.36138781351,100.445119376372,
100.524953214838,100.60869994754,100.692343624556,100.775904368622,100.859402230579,
100.942864731141,101.026309866633,101.109755701476,101.193220296714,101.276773482136,
101.360371315709,101.444102878571,101.523936717037,101.607683449739,101.691327126755,
101.774887870821,101.858385732778,101.941848233341,102.025293368833,102.108739203676,
102.192203798914,102.275756984336,102.359354817908,102.44308638077,102.522920219236,
102.606666951938,102.690310628954,102.77387137302,102.857369234977,102.94083173554,
103.024276871032,103.107722705875,103.191187301113,103.274740486535,103.358338320108,
103.44206988297,103.521903721436,103.663488611563,103.672557568465),
 .UNSPECIFIED.);
#430=B_SPLINE_CURVE_WITH_KNOTS('',3,(#50031,#50032,#50033,#50034,#50035,
#50036,#50037,#50038,#50039,#50040,#50041,#50042,#50043,#50044,#50045,#50046,
#50047,#50048,#50049,#50050,#50051,#50052,#50053,#50054,#50055,#50056,#50057,
#50058,#50059,#50060,#50061,#50062,#50063,#50064,#50065,#50066,#50067,#50068,
#50069,#50070,#50071,#50072,#50073,#50074,#50075,#50076,#50077,#50078,#50079,
#50080,#50081,#50082,#50083,#50084,#50085,#50086,#50087,#50088,#50089,#50090,
#50091,#50092,#50093,#50094,#50095,#50096,#50097,#50098,#50099,#50100,#50101,
#50102,#50103,#50104,#50105,#50106,#50107,#50108,#50109,#50110,#50111,#50112,
#50113,#50114,#50115,#50116,#50117,#50118,#50119,#50120,#50121,#50122,#50123,
#50124,#50125,#50126,#50127,#50128,#50129,#50130,#50131,#50132,#50133,#50134,
#50135,#50136,#50137,#50138,#50139,#50140,#50141,#50142,#50143,#50144,#50145,
#50146,#50147,#50148,#50149,#50150,#50151,#50152,#50153,#50154,#50155,#50156,
#50157,#50158,#50159,#50160,#50161,#50162,#50163,#50164,#50165,#50166,#50167,
#50168,#50169,#50170,#50171,#50172,#50173,#50174,#50175,#50176,#50177,#50178,
#50179,#50180,#50181,#50182,#50183,#50184,#50185,#50186,#50187,#50188,#50189,
#50190,#50191,#50192,#50193,#50194,#50195,#50196,#50197,#50198,#50199,#50200,
#50201,#50202,#50203,#50204,#50205,#50206,#50207,#50208,#50209,#50210,#50211,
#50212,#50213,#50214,#50215,#50216,#50217,#50218,#50219,#50220,#50221,#50222,
#50223,#50224,#50225,#50226,#50227,#50228,#50229,#50230,#50231,#50232,#50233,
#50234,#50235,#50236,#50237,#50238,#50239,#50240,#50241,#50242,#50243,#50244,
#50245,#50246,#50247,#50248,#50249,#50250,#50251,#50252,#50253,#50254,#50255,
#50256,#50257,#50258,#50259),.UNSPECIFIED.,.F.,.F.,(4,3,3,3,3,3,3,3,3,3,
3,3,3,3,3,3,3,3,3,3,3,3,3,3,3,3,3,3,3,3,3,3,3,3,3,3,3,3,3,3,3,3,3,3,3,3,
3,3,3,3,3,3,3,3,3,3,3,3,3,3,3,3,3,3,3,3,3,3,3,3,3,3,3,3,3,3,4),(103.672557568577,
103.754970286827,103.837301170646,103.92274942727,104.004987034183,104.087211884991,
104.169442999906,104.251699402181,104.334043794288,104.416440529236,104.498951993026,
104.520887223635,104.604633956337,104.688277633353,104.771838377419,104.855336239376,
104.938798739939,105.022243875431,105.105689710274,105.189154305512,105.272707490934,
105.356305324506,105.440036887368,105.519870725834,105.603617458536,105.687261135551,
105.770821879618,105.854319741575,105.937782242137,106.021227377629,106.104673212472,
106.18813780771,106.271690993132,106.355288826705,106.439020389567,106.518854228033,
106.602600960735,106.686244637751,106.769805381817,106.853303243773,106.936765744336,
107.020210879828,107.103656714671,107.187121309909,107.270674495331,107.354272328904,
107.438003891766,107.517837730232,107.601584462934,107.68522813995,107.768788884016,
107.852286745973,107.935749246536,108.019194382028,108.102640216871,108.186104812109,
108.269657997531,108.353255831104,108.436987393966,108.516821232431,108.600567965133,
108.684211642149,108.767772386215,108.851270248172,108.934732748735,109.018177884227,
109.10162371907,109.185088314308,109.26864149973,109.352239333302,109.435970896164,
109.515804734631,109.606603297722,109.697095090951,109.787399435718,109.877404147027,
109.955742875523),.UNSPECIFIED.);
#431=B_SPLINE_CURVE_WITH_KNOTS('',3,(#50261,#50262,#50263,#50264,#50265,
#50266,#50267,#50268,#50269,#50270,#50271,#50272,#50273,#50274,#50275,#50276,
#50277,#50278,#50279,#50280,#50281,#50282,#50283,#50284,#50285,#50286,#50287,
#50288,#50289,#50290,#50291,#50292,#50293,#50294,#50295,#50296,#50297,#50298,
#50299,#50300,#50301,#50302,#50303,#50304,#50305,#50306,#50307,#50308,#50309,
#50310,#50311,#50312,#50313,#50314,#50315,#50316,#50317,#50318,#50319,#50320,
#50321,#50322,#50323,#50324,#50325,#50326,#50327,#50328,#50329,#50330,#50331,
#50332,#50333,#50334,#50335,#50336,#50337,#50338,#50339,#50340,#50341,#50342,
#50343,#50344,#50345,#50346,#50347,#50348,#50349,#50350,#50351,#50352,#50353,
#50354,#50355,#50356,#50357,#50358,#50359,#50360,#50361,#50362,#50363,#50364,
#50365,#50366,#50367,#50368,#50369,#50370,#50371,#50372,#50373,#50374,#50375,
#50376,#50377,#50378,#50379,#50380,#50381,#50382,#50383,#50384,#50385,#50386,
#50387,#50388,#50389,#50390,#50391,#50392,#50393,#50394,#50395,#50396,#50397,
#50398,#50399,#50400,#50401,#50402,#50403,#50404,#50405,#50406,#50407,#50408,
#50409,#50410,#50411,#50412,#50413,#50414,#50415,#50416,#50417,#50418,#50419,
#50420,#50421,#50422,#50423,#50424,#50425,#50426,#50427,#50428,#50429,#50430,
#50431,#50432,#50433,#50434,#50435,#50436,#50437,#50438,#50439,#50440,#50441,
#50442,#50443,#50444,#50445,#50446,#50447,#50448,#50449,#50450,#50451,#50452,
#50453,#50454,#50455,#50456,#50457,#50458,#50459,#50460,#50461,#50462,#50463,
#50464,#50465,#50466,#50467,#50468,#50469,#50470,#50471,#50472,#50473,#50474,
#50475,#50476,#50477,#50478,#50479,#50480,#50481,#50482,#50483,#50484,#50485,
#50486,#50487,#50488,#50489),.UNSPECIFIED.,.F.,.F.,(4,3,3,3,3,3,3,3,3,3,
3,3,3,3,3,3,3,3,3,3,3,3,3,3,3,3,3,3,3,3,3,3,3,3,3,3,3,3,3,3,3,3,3,3,3,3,
3,3,3,3,3,3,3,3,3,3,3,3,3,3,3,3,3,3,3,3,3,3,3,3,3,3,3,3,3,3,4),(109.955742875644,
110.041285412932,110.126879716026,110.212540088657,110.298342751316,110.38422432511,
110.47026265263,110.51478823683,110.598534969532,110.682178646548,110.765739390614,
110.849237252571,110.932699753133,111.016144888626,111.099590723469,111.183055318706,
111.266608504128,111.350206337701,111.433937900563,111.513771739029,111.597518471731,
111.681162148746,111.764722892813,111.84822075477,111.931683255332,112.015128390824,
112.098574225667,112.182038820905,112.265592006327,112.3491898399,112.432921402761,
112.512755241228,112.59650197393,112.680145650946,112.763706395012,112.847204256969,
112.930666757531,113.014111893024,113.097557727867,113.181022323104,113.264575508526,
113.348173342099,113.431904904961,113.511738743427,113.595485476129,113.679129153145,
113.762689897211,113.846187759168,113.92965025973,114.013095395222,114.096541230065,
114.180005825303,114.263559010725,114.347156844298,114.43088840716,114.510722245626,
114.594468978328,114.678112655344,114.761673399411,114.845171261368,114.92863376193,
115.012078897423,115.095524732265,115.178989327504,115.262542512926,115.346140346498,
115.42987190936,115.509705747826,115.592661000623,115.675485081759,115.758233684028,
115.840925634918,115.923579714511,116.006234092482,116.08888573277,116.171589700014,
116.238928182824),.UNSPECIFIED.);
#432=B_SPLINE_CURVE_WITH_KNOTS('',3,(#50491,#50492,#50493,#50494,#50495,
#50496,#50497,#50498,#50499,#50500,#50501,#50502,#50503,#50504,#50505,#50506,
#50507,#50508,#50509,#50510,#50511,#50512,#50513,#50514,#50515,#50516,#50517,
#50518,#50519,#50520,#50521,#50522,#50523,#50524,#50525,#50526,#50527,#50528,
#50529,#50530,#50531,#50532,#50533,#50534,#50535,#50536,#50537,#50538,#50539,
#50540,#50541,#50542,#50543,#50544,#50545,#50546,#50547,#50548,#50549,#50550,
#50551,#50552,#50553,#50554,#50555,#50556,#50557,#50558,#50559,#50560,#50561,
#50562,#50563,#50564,#50565,#50566,#50567,#50568,#50569,#50570,#50571,#50572,
#50573,#50574,#50575,#50576,#50577,#50578,#50579,#50580,#50581,#50582,#50583,
#50584,#50585,#50586,#50587,#50588,#50589,#50590,#50591,#50592,#50593,#50594,
#50595,#50596,#50597,#50598,#50599,#50600,#50601,#50602,#50603,#50604,#50605,
#50606,#50607,#50608,#50609,#50610,#50611,#50612,#50613,#50614,#50615,#50616,
#50617,#50618,#50619,#50620,#50621,#50622,#50623,#50624,#50625,#50626,#50627,
#50628,#50629,#50630,#50631,#50632,#50633,#50634,#50635,#50636,#50637,#50638,
#50639,#50640,#50641,#50642,#50643,#50644,#50645,#50646,#50647,#50648,#50649,
#50650,#50651,#50652,#50653,#50654,#50655,#50656,#50657,#50658,#50659,#50660,
#50661,#50662,#50663,#50664,#50665,#50666,#50667,#50668,#50669,#50670,#50671,
#50672,#50673,#50674,#50675,#50676,#50677,#50678,#50679,#50680,#50681,#50682,
#50683,#50684,#50685,#50686,#50687,#50688,#50689,#50690,#50691,#50692,#50693,
#50694,#50695,#50696,#50697,#50698,#50699,#50700,#50701,#50702,#50703,#50704,
#50705,#50706,#50707,#50708,#50709,#50710,#50711,#50712,#50713,#50714,#50715,
#50716,#50717,#50718,#50719),.UNSPECIFIED.,.F.,.F.,(4,3,3,3,3,3,3,3,3,3,
3,3,3,3,3,3,3,3,3,3,3,3,3,3,3,3,3,3,3,3,3,3,3,3,3,3,3,3,3,3,3,3,3,3,3,3,
3,3,3,3,3,3,3,3,3,3,3,3,3,3,3,3,3,3,3,3,3,3,3,3,3,3,3,3,3,3,4),(116.238928183003,
116.343160711796,116.449245634065,116.508689250025,116.592435982727,116.676079659743,
116.759640403809,116.843138265766,116.926600766328,117.010045901821,117.093491736663,
117.176956331901,117.260509517323,117.344107350896,117.427838913757,117.507672752224,
117.591419484926,117.675063161942,117.758623906008,117.842121767965,117.925584268528,
118.00902940402,118.092475238863,118.175939834101,118.259493019523,118.343090853096,
118.426822415957,118.506656254423,118.590402987125,118.674046664141,118.757607408207,
118.841105270164,118.924567770726,119.008012906218,119.091458741061,119.174923336299,
119.258476521721,119.342074355293,119.425805918155,119.505639756622,119.589386489324,
119.67303016634,119.756590910406,119.840088772363,119.923551272925,120.006996408418,
120.090442243261,120.173906838499,120.25746002392,120.341057857493,120.424789420355,
120.504623258821,120.588369991523,120.672013668539,120.755574412605,120.839072274562,
120.922534775125,121.005979910617,121.08942574546,121.172890340698,121.25644352612,
121.340041359693,121.423772922555,121.50360676102,121.587353493722,121.670997170738,
121.754557914805,121.838055776761,121.921518277324,122.004963412816,122.088409247659,
122.171873842898,122.255427028319,122.339024861892,122.422756424754,122.50259026322,
122.522113490003),.UNSPECIFIED.);
#433=B_SPLINE_CURVE_WITH_KNOTS('',3,(#50721,#50722,#50723,#50724,#50725,
#50726,#50727,#50728,#50729,#50730,#50731,#50732,#50733,#50734,#50735,#50736,
#50737,#50738,#50739,#50740,#50741,#50742,#50743,#50744,#50745,#50746,#50747,
#50748,#50749,#50750,#50751,#50752,#50753,#50754,#50755,#50756,#50757,#50758,
#50759,#50760,#50761,#50762,#50763,#50764,#50765,#50766,#50767,#50768,#50769,
#50770,#50771,#50772,#50773,#50774,#50775,#50776,#50777,#50778,#50779,#50780,
#50781,#50782,#50783,#50784,#50785,#50786,#50787,#50788,#50789,#50790,#50791,
#50792,#50793,#50794,#50795,#50796,#50797,#50798,#50799,#50800,#50801,#50802,
#50803,#50804,#50805,#50806,#50807,#50808,#50809,#50810,#50811,#50812,#50813,
#50814,#50815,#50816,#50817,#50818,#50819,#50820,#50821,#50822,#50823,#50824,
#50825,#50826,#50827,#50828,#50829,#50830,#50831,#50832,#50833,#50834,#50835,
#50836,#50837,#50838,#50839,#50840,#50841,#50842,#50843,#50844,#50845,#50846,
#50847,#50848,#50849,#50850,#50851,#50852,#50853,#50854,#50855,#50856,#50857,
#50858,#50859,#50860,#50861,#50862,#50863,#50864,#50865,#50866,#50867,#50868,
#50869,#50870,#50871,#50872,#50873,#50874,#50875,#50876,#50877,#50878,#50879,
#50880,#50881,#50882,#50883,#50884,#50885,#50886,#50887,#50888,#50889,#50890,
#50891,#50892,#50893,#50894,#50895,#50896,#50897,#50898,#50899,#50900,#50901,
#50902,#50903,#50904,#50905,#50906,#50907,#50908,#50909,#50910,#50911,#50912,
#50913,#50914,#50915,#50916,#50917,#50918,#50919,#50920,#50921,#50922,#50923,
#50924,#50925,#50926,#50927,#50928,#50929,#50930,#50931,#50932,#50933,#50934,
#50935,#50936,#50937,#50938,#50939,#50940,#50941,#50942,#50943,#50944,#50945,
#50946),.UNSPECIFIED.,.F.,.F.,(4,3,3,3,3,3,3,3,3,3,3,3,3,3,3,3,3,3,3,3,
3,3,3,3,3,3,3,3,3,3,3,3,3,3,3,3,3,3,3,3,3,3,3,3,3,3,3,3,3,3,3,3,3,3,3,3,
3,3,3,3,3,3,3,3,3,3,3,3,3,3,3,3,3,3,3,4),(122.522113490184,122.605579195225,
122.688942451667,122.772223670943,122.855443190419,122.9386291599,123.021799364267,
123.104972125662,123.188165764287,123.271448247297,123.354777772417,123.438235782967,
123.501573765419,123.585320498121,123.668964175137,123.752524919203,123.83602278116,
123.919485281723,124.002930417215,124.086376252058,124.169840847296,124.253394032718,
124.33699186629,124.420723429152,124.500557267618,124.58430400032,124.667947677336,
124.751508421402,124.835006283359,124.918468783921,125.001913919414,125.085359754256,
125.168824349494,125.252377534916,125.335975368489,125.419706931351,125.499540769817,
125.583287502519,125.666931179535,125.750491923601,125.833989785557,125.91745228612,
126.000897421612,126.084343256455,126.167807851693,126.251361037115,126.334958870688,
126.41869043355,126.498524272016,126.582271004718,126.665914681734,126.7494754258,
126.832973287757,126.916435788319,126.999880923812,127.083326758655,127.166791353893,
127.250344539315,127.333942372887,127.417673935749,127.497507774215,127.581254506917,
127.664898183933,127.748458927999,127.831956789956,127.915419290518,127.99886442601,
128.082310260853,128.165774856091,128.249328041513,128.332925875085,128.416657437947,
128.496491276415,128.597476601312,128.701387699168,128.805298797024),
 .UNSPECIFIED.);
#434=B_SPLINE_CURVE_WITH_KNOTS('',3,(#50948,#50949,#50950,#50951,#50952,
#50953,#50954,#50955,#50956,#50957,#50958,#50959,#50960,#50961,#50962,#50963,
#50964,#50965,#50966,#50967,#50968,#50969,#50970,#50971,#50972,#50973,#50974,
#50975,#50976,#50977,#50978,#50979,#50980,#50981,#50982,#50983,#50984,#50985,
#50986,#50987,#50988,#50989,#50990,#50991,#50992,#50993,#50994,#50995,#50996,
#50997,#50998,#50999,#51000,#51001,#51002,#51003,#51004,#51005,#51006,#51007,
#51008,#51009,#51010,#51011,#51012,#51013,#51014,#51015,#51016,#51017,#51018,
#51019,#51020,#51021,#51022,#51023,#51024,#51025,#51026,#51027,#51028,#51029,
#51030,#51031,#51032,#51033,#51034,#51035,#51036,#51037,#51038,#51039,#51040,
#51041,#51042,#51043,#51044,#51045,#51046,#51047,#51048,#51049,#51050,#51051,
#51052,#51053,#51054,#51055,#51056,#51057,#51058,#51059,#51060,#51061,#51062,
#51063,#51064,#51065,#51066,#51067,#51068,#51069,#51070,#51071,#51072,#51073,
#51074,#51075,#51076,#51077,#51078,#51079,#51080,#51081,#51082,#51083,#51084,
#51085,#51086,#51087,#51088,#51089,#51090,#51091,#51092,#51093,#51094,#51095,
#51096,#51097,#51098,#51099,#51100,#51101,#51102,#51103,#51104,#51105,#51106,
#51107,#51108,#51109,#51110,#51111,#51112,#51113,#51114,#51115,#51116,#51117,
#51118,#51119,#51120,#51121,#51122,#51123,#51124,#51125,#51126,#51127,#51128,
#51129,#51130,#51131,#51132,#51133,#51134,#51135,#51136,#51137,#51138,#51139,
#51140,#51141,#51142,#51143,#51144,#51145,#51146,#51147,#51148,#51149,#51150,
#51151,#51152,#51153,#51154,#51155,#51156,#51157,#51158,#51159,#51160,#51161,
#51162,#51163,#51164,#51165,#51166,#51167,#51168,#51169,#51170,#51171,#51172,
#51173,#51174,#51175,#51176),.UNSPECIFIED.,.F.,.F.,(4,3,3,3,3,3,3,3,3,3,
3,3,3,3,3,3,3,3,3,3,3,3,3,3,3,3,3,3,3,3,3,3,3,3,3,3,3,3,3,3,3,3,3,3,3,3,
3,3,3,3,3,3,3,3,3,3,3,3,3,3,3,3,3,3,3,3,3,3,3,3,3,3,3,3,3,3,4),(128.805298797183,
128.891570794862,128.974631964316,129.057688587614,129.140759045218,129.223861723451,
129.307060779198,129.390317093249,129.473693556952,129.495474778614,129.579221511316,
129.662865188332,129.746425932398,129.829923794355,129.913386294917,129.99683143041,
130.080277265252,130.16374186049,130.247295045912,130.330892879485,130.414624442347,
130.494458280813,130.578205013515,130.661848690531,130.745409434597,130.828907296554,
130.912369797116,130.995814932609,131.079260767451,131.162725362689,131.246278548111,
131.329876381684,131.413607944546,131.493441783012,131.577188515714,131.66083219273,
131.744392936796,131.827890798753,131.911353299316,131.994798434808,132.078244269651,
132.161708864889,132.245262050311,132.328859883883,132.412591446745,132.492425285211,
132.576172017913,132.659815694929,132.743376438995,132.826874300952,132.910336801515,
132.993781937007,133.07722777185,133.160692367088,133.24424555251,133.327843386082,
133.411574948944,133.49140878741,133.575155520112,133.658799197128,133.742359941194,
133.825857803151,133.909320303714,133.992765439206,134.076211274048,134.159675869286,
134.243229054708,134.326826888281,134.410558451143,134.49039228961,134.575400498315,
134.660296053933,134.745095496624,134.830942648559,134.915588822726,135.002036463545,
135.088484104363),.UNSPECIFIED.);
#435=B_SPLINE_CURVE_WITH_KNOTS('',3,(#51178,#51179,#51180,#51181,#51182,
#51183,#51184,#51185,#51186,#51187,#51188,#51189,#51190,#51191,#51192,#51193,
#51194,#51195,#51196,#51197,#51198,#51199,#51200,#51201,#51202,#51203,#51204,
#51205,#51206,#51207,#51208,#51209,#51210,#51211,#51212,#51213,#51214,#51215,
#51216,#51217,#51218,#51219,#51220,#51221,#51222,#51223,#51224,#51225,#51226,
#51227,#51228,#51229,#51230,#51231,#51232,#51233,#51234,#51235,#51236,#51237,
#51238,#51239,#51240,#51241,#51242,#51243,#51244,#51245,#51246,#51247,#51248,
#51249,#51250,#51251,#51252,#51253,#51254,#51255,#51256,#51257,#51258,#51259,
#51260,#51261,#51262,#51263,#51264,#51265,#51266,#51267,#51268,#51269,#51270,
#51271,#51272,#51273,#51274,#51275,#51276,#51277,#51278,#51279,#51280,#51281,
#51282,#51283,#51284,#51285,#51286,#51287,#51288,#51289,#51290,#51291,#51292,
#51293,#51294,#51295,#51296,#51297,#51298,#51299,#51300,#51301,#51302,#51303,
#51304,#51305,#51306,#51307,#51308,#51309,#51310,#51311,#51312,#51313,#51314,
#51315,#51316,#51317,#51318,#51319,#51320,#51321,#51322,#51323,#51324,#51325,
#51326,#51327,#51328,#51329,#51330,#51331,#51332,#51333,#51334,#51335,#51336,
#51337,#51338,#51339,#51340,#51341,#51342,#51343,#51344,#51345,#51346,#51347,
#51348,#51349,#51350,#51351,#51352,#51353,#51354,#51355,#51356,#51357,#51358,
#51359,#51360,#51361,#51362,#51363,#51364,#51365,#51366,#51367,#51368,#51369,
#51370,#51371,#51372,#51373,#51374,#51375,#51376,#51377,#51378,#51379,#51380,
#51381,#51382,#51383,#51384,#51385,#51386,#51387,#51388,#51389,#51390,#51391,
#51392,#51393,#51394,#51395,#51396,#51397,#51398,#51399,#51400,#51401,#51402,
#51403,#51404,#51405,#51406),.UNSPECIFIED.,.F.,.F.,(4,3,3,3,3,3,3,3,3,3,
3,3,3,3,3,3,3,3,3,3,3,3,3,3,3,3,3,3,3,3,3,3,3,3,3,3,3,3,3,3,3,3,3,3,3,3,
3,3,3,3,3,3,3,3,3,3,3,3,3,3,3,3,3,3,3,3,3,3,3,3,3,3,3,3,3,3,4),(135.088484104542,
135.180495486085,135.272995115929,135.365747177429,135.458831781584,135.489375791809,
135.573122524511,135.656766201527,135.740326945593,135.82382480755,135.907287308113,
135.990732443605,136.074178278448,136.157642873686,136.241196059108,136.324793892681,
136.408525455543,136.488359294008,136.57210602671,136.655749703726,136.739310447792,
136.822808309749,136.906270810311,136.989715945804,137.073161780647,137.156626375885,
137.240179561306,137.323777394879,137.407508957741,137.487342796207,137.571089528909,
137.654733205925,137.738293949991,137.821791811948,137.90525431251,137.988699448003,
138.072145282845,138.155609878084,138.239163063505,138.322760897078,138.40649245994,
138.486326298406,138.570073031108,138.653716708124,138.73727745219,138.820775314147,
138.90423781471,138.987682950202,139.071128785045,139.154593380283,139.238146565705,
139.321744399278,139.405475962139,139.485309800605,139.569056533307,139.652700210323,
139.736260954389,139.819758816346,139.903221316909,139.986666452401,140.070112287244,
140.153576882482,140.237130067904,140.320727901477,140.404459464339,140.484293302805,
140.566929223367,140.649462929782,140.731915551088,140.814307347838,140.896666824531,
140.979012936728,141.061364626536,141.143783535083,141.226237338813,141.308802211266,
141.371669411407),.UNSPECIFIED.);
#436=B_SPLINE_CURVE_WITH_KNOTS('',3,(#51408,#51409,#51410,#51411,#51412,
#51413,#51414,#51415,#51416,#51417,#51418,#51419,#51420,#51421,#51422,#51423,
#51424,#51425,#51426,#51427,#51428,#51429,#51430,#51431,#51432,#51433,#51434,
#51435,#51436,#51437,#51438,#51439,#51440,#51441,#51442,#51443,#51444,#51445,
#51446,#51447,#51448,#51449,#51450,#51451,#51452,#51453,#51454,#51455,#51456,
#51457,#51458,#51459,#51460,#51461,#51462,#51463,#51464,#51465,#51466,#51467,
#51468,#51469,#51470,#51471,#51472,#51473,#51474,#51475,#51476,#51477,#51478,
#51479,#51480,#51481,#51482,#51483,#51484,#51485,#51486,#51487,#51488,#51489,
#51490,#51491,#51492,#51493,#51494,#51495,#51496,#51497,#51498,#51499,#51500,
#51501,#51502,#51503,#51504,#51505,#51506,#51507,#51508,#51509,#51510,#51511,
#51512,#51513,#51514,#51515,#51516,#51517,#51518,#51519,#51520,#51521,#51522,
#51523,#51524,#51525,#51526,#51527,#51528,#51529,#51530,#51531,#51532,#51533,
#51534,#51535,#51536,#51537,#51538,#51539,#51540,#51541,#51542,#51543,#51544,
#51545,#51546,#51547,#51548,#51549,#51550,#51551,#51552,#51553,#51554,#51555,
#51556,#51557,#51558,#51559,#51560,#51561,#51562,#51563,#51564,#51565,#51566,
#51567,#51568,#51569,#51570,#51571,#51572,#51573,#51574,#51575,#51576,#51577,
#51578,#51579,#51580,#51581,#51582,#51583,#51584,#51585,#51586,#51587,#51588,
#51589,#51590,#51591,#51592,#51593,#51594,#51595,#51596,#51597,#51598,#51599,
#51600,#51601,#51602,#51603,#51604,#51605,#51606,#51607,#51608,#51609,#51610,
#51611,#51612,#51613,#51614,#51615,#51616,#51617,#51618,#51619,#51620,#51621,
#51622,#51623,#51624,#51625,#51626,#51627,#51628,#51629,#51630,#51631,#51632,
#51633),.UNSPECIFIED.,.F.,.F.,(4,3,3,3,3,3,3,3,3,3,3,3,3,3,3,3,3,3,3,3,
3,3,3,3,3,3,3,3,3,3,3,3,3,3,3,3,3,3,3,3,3,3,3,3,3,3,3,3,3,3,3,3,3,3,3,3,
3,3,3,3,3,3,3,3,3,3,3,3,3,3,3,3,3,3,3,4),(141.371669411542,141.483276805004,
141.567023537706,141.650667214722,141.734227958788,141.817725820745,141.901188321307,
141.984633456799,142.068079291642,142.15154388688,142.235097072302,142.318694905875,
142.402426468736,142.482260307203,142.566007039905,142.649650716921,142.733211460987,
142.816709322944,142.900171823506,142.983616958999,143.067062793841,143.150527389079,
143.234080574501,143.317678408074,143.401409970936,143.481243809402,143.564990542104,
143.64863421912,143.732194963186,143.815692825143,143.899155325705,143.982600461198,
144.066046296041,144.149510891279,144.233064076701,144.316661910273,144.400393473135,
144.480227311601,144.563974044303,144.647617721319,144.731178465385,144.814676327342,
144.898138827905,144.981583963397,145.06502979824,145.148494393478,145.2320475789,
145.315645412473,145.399376975334,145.4792108138,145.562957546502,145.646601223518,
145.730161967584,145.813659829541,145.897122330104,145.980567465596,146.064013300439,
146.147477895677,146.231031081099,146.314628914672,146.398360477534,146.478194316,
146.561941048702,146.645584725718,146.729145469785,146.812643331741,146.896105832304,
146.979550967796,147.062996802639,147.146461397878,147.2300145833,147.313612416872,
147.397343979734,147.477177818199,147.605135855273,147.654854718722),
 .UNSPECIFIED.);
#437=B_SPLINE_CURVE_WITH_KNOTS('',3,(#51635,#51636,#51637,#51638,#51639,
#51640,#51641,#51642,#51643,#51644,#51645,#51646,#51647,#51648,#51649,#51650,
#51651,#51652,#51653,#51654,#51655,#51656,#51657,#51658,#51659,#51660,#51661,
#51662,#51663,#51664,#51665,#51666,#51667,#51668,#51669,#51670,#51671,#51672,
#51673,#51674,#51675,#51676,#51677,#51678,#51679,#51680,#51681,#51682,#51683,
#51684,#51685,#51686,#51687,#51688,#51689,#51690,#51691,#51692,#51693,#51694,
#51695,#51696,#51697,#51698,#51699,#51700,#51701,#51702,#51703,#51704,#51705,
#51706,#51707,#51708,#51709,#51710,#51711,#51712,#51713,#51714,#51715,#51716,
#51717,#51718,#51719,#51720,#51721,#51722,#51723,#51724,#51725,#51726,#51727,
#51728,#51729,#51730,#51731,#51732,#51733,#51734,#51735,#51736,#51737,#51738,
#51739,#51740,#51741,#51742,#51743,#51744,#51745,#51746,#51747,#51748,#51749,
#51750,#51751,#51752,#51753,#51754,#51755,#51756,#51757,#51758,#51759,#51760,
#51761,#51762,#51763,#51764,#51765,#51766,#51767,#51768,#51769,#51770,#51771,
#51772,#51773,#51774,#51775,#51776,#51777,#51778,#51779,#51780,#51781,#51782,
#51783,#51784,#51785,#51786,#51787,#51788,#51789,#51790,#51791,#51792,#51793,
#51794,#51795,#51796,#51797,#51798,#51799,#51800,#51801,#51802,#51803,#51804,
#51805,#51806,#51807,#51808,#51809,#51810,#51811,#51812,#51813,#51814,#51815,
#51816,#51817,#51818,#51819,#51820,#51821,#51822,#51823,#51824,#51825,#51826,
#51827,#51828,#51829,#51830,#51831,#51832,#51833,#51834,#51835,#51836,#51837,
#51838,#51839,#51840,#51841,#51842,#51843,#51844,#51845,#51846,#51847,#51848,
#51849,#51850,#51851,#51852,#51853,#51854,#51855,#51856,#51857,#51858,#51859,
#51860,#51861,#51862,#51863),.UNSPECIFIED.,.F.,.F.,(4,3,3,3,3,3,3,3,3,3,
3,3,3,3,3,3,3,3,3,3,3,3,3,3,3,3,3,3,3,3,3,3,3,3,3,3,3,3,3,3,3,3,3,3,3,3,
3,3,3,3,3,3,3,3,3,3,3,3,3,3,3,3,3,3,3,3,3,3,3,3,3,3,3,3,3,3,4),(147.654854718883,
147.737228180291,147.819526616244,147.901774471423,147.983995941504,148.066210060611,
148.148435854635,148.230742693763,148.313089645585,148.395567187923,148.476161320398,
148.5599080531,148.643551730116,148.727112474182,148.810610336139,148.894072836702,
148.977517972194,149.060963807037,149.144428402275,149.227981587696,149.311579421269,
149.395310984131,149.475144822597,149.558891555299,149.642535232315,149.726095976381,
149.809593838338,149.893056338901,149.976501474393,150.059947309236,150.143411904474,
150.226965089896,150.310562923469,150.394294486331,150.474128324796,150.557875057498,
150.641518734514,150.72507947858,150.808577340537,150.8920398411,150.975484976592,
151.058930811435,151.142395406672,151.225948592094,151.309546425667,151.393277988528,
151.473111826995,151.556858559697,151.640502236713,151.72406298078,151.807560842736,
151.891023343299,151.974468478792,152.057914313635,152.141378908873,152.224932094295,
152.308529927868,152.39226149073,152.472095329195,152.555842061897,152.639485738913,
152.723046482979,152.806544344935,152.890006845498,152.97345198099,153.056897815833,
153.140362411071,153.223915596493,153.307513430065,153.391244992927,153.471078831394,
153.560529790671,153.649805113436,153.738836835757,153.827717004931,153.916394555608,
153.938040025764),.UNSPECIFIED.);
#438=B_SPLINE_CURVE_WITH_KNOTS('',3,(#51865,#51866,#51867,#51868,#51869,
#51870,#51871,#51872,#51873,#51874,#51875,#51876,#51877,#51878,#51879,#51880,
#51881,#51882,#51883,#51884,#51885,#51886,#51887,#51888,#51889,#51890,#51891,
#51892,#51893,#51894,#51895,#51896,#51897,#51898,#51899,#51900,#51901,#51902,
#51903,#51904,#51905,#51906,#51907,#51908,#51909,#51910,#51911,#51912,#51913,
#51914,#51915,#51916,#51917,#51918,#51919,#51920,#51921,#51922,#51923,#51924,
#51925,#51926,#51927,#51928,#51929,#51930,#51931,#51932,#51933,#51934,#51935,
#51936,#51937,#51938,#51939,#51940,#51941,#51942,#51943,#51944,#51945,#51946,
#51947,#51948,#51949,#51950,#51951,#51952,#51953,#51954,#51955,#51956,#51957,
#51958,#51959,#51960,#51961,#51962,#51963,#51964,#51965,#51966,#51967,#51968,
#51969,#51970,#51971,#51972,#51973,#51974,#51975,#51976,#51977,#51978,#51979,
#51980,#51981,#51982,#51983,#51984,#51985,#51986,#51987,#51988,#51989,#51990,
#51991,#51992,#51993,#51994,#51995,#51996,#51997,#51998,#51999,#52000,#52001,
#52002,#52003,#52004,#52005,#52006,#52007,#52008,#52009,#52010,#52011,#52012,
#52013,#52014,#52015,#52016,#52017,#52018,#52019,#52020,#52021,#52022,#52023,
#52024,#52025,#52026,#52027,#52028,#52029,#52030,#52031,#52032,#52033,#52034,
#52035,#52036,#52037,#52038,#52039,#52040,#52041,#52042,#52043,#52044,#52045,
#52046,#52047,#52048,#52049,#52050,#52051,#52052,#52053,#52054,#52055,#52056,
#52057,#52058,#52059,#52060,#52061,#52062,#52063,#52064,#52065,#52066,#52067,
#52068,#52069,#52070,#52071,#52072,#52073,#52074,#52075,#52076,#52077,#52078,
#52079,#52080,#52081,#52082,#52083,#52084,#52085,#52086,#52087,#52088,#52089,
#52090,#52091,#52092,#52093,#52094,#52095,#52096),.UNSPECIFIED.,.F.,.F.,
(4,3,3,3,3,3,3,3,3,3,3,3,3,3,3,3,3,3,3,3,3,3,3,3,3,3,3,3,3,3,3,3,3,3,3,
3,3,3,3,3,3,3,3,3,3,3,3,3,3,3,3,3,3,3,3,3,3,3,3,3,3,3,3,3,3,3,3,3,3,3,3,
3,3,3,3,3,3,4),(153.938040025901,154.024359782887,154.110756324578,154.200582826831,
154.287234368446,154.373981223819,154.460883689602,154.470062333593,154.553809066295,
154.637452743311,154.721013487377,154.804511349334,154.887973849897,154.971418985389,
155.054864820232,155.13832941547,155.221882600892,155.305480434464,155.389211997326,
155.469045835792,155.552792568494,155.636436245509,155.719996989576,155.803494851533,
155.886957352095,155.970402487588,156.05384832243,156.137312917668,156.22086610309,
156.304463936663,156.388195499525,156.468029337991,156.551776070693,156.635419747709,
156.718980491775,156.802478353732,156.885940854295,156.969385989787,157.05283182463,
157.136296419867,157.219849605289,157.303447438862,157.387179001724,157.46701284019,
157.550759572892,157.634403249908,157.717963993974,157.80146185593,157.884924356493,
157.968369491985,158.051815326828,158.135279922066,158.218833107488,158.302430941061,
158.386162503922,158.46599634239,158.549743075092,158.633386752108,158.716947496174,
158.800445358131,158.883907858694,158.967352994187,159.05079882903,159.134263424268,
159.21781660969,159.301414443262,159.385146006124,159.464979844589,159.547722225675,
159.631910114101,159.714449093052,159.796933736485,159.87938296901,159.964843560028,
160.047301191615,160.129775716868,160.212308983891,160.221225333081),
 .UNSPECIFIED.);
#439=B_SPLINE_CURVE_WITH_KNOTS('',3,(#52098,#52099,#52100,#52101,#52102,
#52103,#52104,#52105,#52106,#52107,#52108,#52109,#52110,#52111,#52112,#52113,
#52114,#52115,#52116,#52117,#52118,#52119,#52120,#52121,#52122,#52123,#52124,
#52125,#52126,#52127,#52128,#52129,#52130,#52131,#52132,#52133,#52134,#52135,
#52136,#52137,#52138,#52139,#52140,#52141,#52142,#52143,#52144,#52145,#52146,
#52147,#52148,#52149,#52150,#52151,#52152,#52153,#52154,#52155,#52156,#52157,
#52158,#52159,#52160,#52161,#52162,#52163,#52164,#52165,#52166,#52167,#52168,
#52169,#52170,#52171,#52172,#52173,#52174,#52175,#52176,#52177,#52178,#52179,
#52180,#52181,#52182,#52183,#52184,#52185,#52186,#52187,#52188,#52189,#52190,
#52191,#52192,#52193,#52194,#52195,#52196,#52197,#52198,#52199,#52200,#52201,
#52202,#52203,#52204,#52205,#52206,#52207,#52208,#52209,#52210,#52211,#52212,
#52213,#52214,#52215,#52216,#52217,#52218,#52219,#52220,#52221,#52222,#52223,
#52224,#52225,#52226,#52227,#52228,#52229,#52230,#52231,#52232,#52233,#52234,
#52235,#52236,#52237,#52238,#52239,#52240,#52241,#52242,#52243,#52244,#52245,
#52246,#52247,#52248,#52249,#52250,#52251,#52252,#52253,#52254,#52255,#52256,
#52257,#52258,#52259,#52260,#52261,#52262,#52263,#52264,#52265,#52266,#52267,
#52268,#52269,#52270,#52271,#52272,#52273,#52274,#52275,#52276,#52277,#52278,
#52279,#52280,#52281,#52282,#52283,#52284,#52285,#52286,#52287,#52288,#52289,
#52290,#52291,#52292,#52293,#52294,#52295,#52296,#52297,#52298,#52299,#52300,
#52301,#52302,#52303,#52304,#52305,#52306,#52307,#52308,#52309,#52310,#52311,
#52312,#52313,#52314,#52315,#52316,#52317,#52318,#52319,#52320,#52321,#52322,
#52323,#52324,#52325,#52326),.UNSPECIFIED.,.F.,.F.,(4,3,3,3,3,3,3,3,3,3,
3,3,3,3,3,3,3,3,3,3,3,3,3,3,3,3,3,3,3,3,3,3,3,3,3,3,3,3,3,3,3,3,3,3,3,3,
3,3,3,3,3,3,3,3,3,3,3,3,3,3,3,3,3,3,3,3,3,3,3,3,3,3,3,3,3,3,4),(160.221225333185,
160.329604730348,160.44063773956,160.463963346788,160.54771007949,160.631353756506,
160.714914500572,160.798412362529,160.881874863091,160.965319998584,161.048765833426,
161.132230428665,161.215783614086,161.299381447659,161.383113010521,161.462946848987,
161.546693581689,161.630337258705,161.713898002771,161.797395864728,161.88085836529,
161.964303500783,162.047749335625,162.131213930863,162.214767116285,162.298364949858,
162.38209651272,162.461930351186,162.545677083888,162.629320760904,162.71288150497,
162.796379366927,162.87984186749,162.963287002982,163.046732837825,163.130197433063,
163.213750618485,163.297348452058,163.38108001492,163.460913853385,163.544660586087,
163.628304263103,163.711865007169,163.795362869126,163.878825369689,163.962270505181,
164.045716340024,164.129180935262,164.212734120684,164.296331954257,164.380063517119,
164.459897355585,164.543644088287,164.627287765303,164.710848509369,164.794346371326,
164.877808871889,164.961254007381,165.044699842224,165.128164437462,165.211717622884,
165.295315456457,165.379047019319,165.458880857784,165.542627590486,165.626271267502,
165.709832011568,165.793329873525,165.876792374087,165.960237509579,166.043683344422,
166.12714793966,166.210701125082,166.294298958654,166.378030521516,166.457864359983,
166.50441064026),.UNSPECIFIED.);
#440=B_SPLINE_CURVE_WITH_KNOTS('',3,(#52328,#52329,#52330,#52331,#52332,
#52333,#52334,#52335,#52336,#52337,#52338,#52339,#52340,#52341,#52342,#52343,
#52344,#52345,#52346,#52347,#52348,#52349,#52350,#52351,#52352,#52353,#52354,
#52355,#52356,#52357,#52358,#52359,#52360,#52361,#52362,#52363,#52364,#52365,
#52366,#52367,#52368,#52369,#52370,#52371,#52372,#52373,#52374,#52375,#52376,
#52377,#52378,#52379,#52380,#52381,#52382,#52383,#52384,#52385,#52386,#52387,
#52388,#52389,#52390,#52391,#52392,#52393,#52394,#52395,#52396,#52397,#52398,
#52399,#52400,#52401,#52402,#52403,#52404,#52405,#52406,#52407,#52408,#52409,
#52410,#52411,#52412,#52413,#52414,#52415,#52416,#52417,#52418,#52419,#52420,
#52421,#52422,#52423,#52424,#52425,#52426,#52427,#52428,#52429,#52430,#52431,
#52432,#52433,#52434,#52435,#52436,#52437,#52438,#52439,#52440,#52441,#52442,
#52443,#52444,#52445,#52446,#52447,#52448,#52449,#52450,#52451,#52452,#52453,
#52454,#52455,#52456,#52457,#52458,#52459,#52460,#52461,#52462,#52463,#52464,
#52465,#52466,#52467,#52468,#52469,#52470,#52471,#52472,#52473,#52474,#52475,
#52476,#52477,#52478,#52479,#52480,#52481,#52482,#52483,#52484,#52485,#52486,
#52487,#52488,#52489,#52490,#52491,#52492,#52493,#52494,#52495,#52496,#52497,
#52498,#52499,#52500,#52501,#52502,#52503,#52504,#52505,#52506,#52507,#52508,
#52509,#52510,#52511,#52512,#52513,#52514,#52515,#52516,#52517,#52518,#52519,
#52520,#52521,#52522,#52523,#52524,#52525,#52526,#52527,#52528,#52529,#52530,
#52531,#52532,#52533,#52534,#52535,#52536,#52537,#52538,#52539,#52540,#52541,
#52542,#52543,#52544,#52545,#52546,#52547,#52548,#52549,#52550,#52551,#52552,
#52553,#52554,#52555,#52556),.UNSPECIFIED.,.F.,.F.,(4,3,3,3,3,3,3,3,3,3,
3,3,3,3,3,3,3,3,3,3,3,3,3,3,3,3,3,3,3,3,3,3,3,3,3,3,3,3,3,3,3,3,3,3,3,3,
3,3,3,3,3,3,3,3,3,3,3,3,3,3,3,3,3,3,3,3,3,3,3,3,3,3,3,3,3,3,4),(166.504410640448,
166.587541388229,166.670571858568,166.753522758781,166.836414719578,166.919276960235,
167.002126467252,167.084981829367,167.167861636136,167.250831058329,167.333851236403,
167.416992715462,167.456847862182,167.540594594884,167.6242382719,167.707799015966,
167.791296877923,167.874759378485,167.958204513978,168.04165034882,168.125114944059,
168.20866812948,168.292265963053,168.375997525915,168.455831364381,168.539578097083,
168.623221774099,168.706782518165,168.790280380122,168.873742880685,168.957188016177,
169.04063385102,169.124098446258,169.20765163168,169.291249465253,169.374981028115,
169.45481486658,169.538561599282,169.622205276298,169.705766020364,169.789263882321,
169.872726382884,169.956171518376,170.039617353219,170.123081948457,170.206635133879,
170.290232967452,170.373964530313,170.45379836878,170.537545101482,170.621188778498,
170.704749522565,170.788247384521,170.871709885084,170.955155020576,171.038600855419,
171.122065450657,171.205618636079,171.289216469651,171.372948032513,171.452781870979,
171.536528603681,171.620172280696,171.703733024763,171.78723088672,171.870693387282,
171.954138522775,172.037584357617,172.121048952855,172.204602138277,172.28819997185,
172.371931534711,172.451765373178,172.549892717309,172.647579141693,172.744447331875,
172.787595947253),.UNSPECIFIED.);
#441=B_SPLINE_CURVE_WITH_KNOTS('',3,(#52558,#52559,#52560,#52561,#52562,
#52563,#52564,#52565,#52566,#52567,#52568,#52569,#52570,#52571,#52572,#52573,
#52574,#52575,#52576,#52577,#52578,#52579,#52580,#52581,#52582,#52583,#52584,
#52585,#52586,#52587,#52588,#52589,#52590,#52591,#52592,#52593,#52594,#52595,
#52596,#52597,#52598,#52599,#52600,#52601,#52602,#52603,#52604,#52605,#52606,
#52607,#52608,#52609,#52610,#52611,#52612,#52613,#52614,#52615,#52616,#52617,
#52618,#52619,#52620,#52621,#52622,#52623,#52624,#52625,#52626,#52627,#52628,
#52629,#52630,#52631,#52632,#52633,#52634,#52635,#52636,#52637,#52638,#52639,
#52640,#52641,#52642,#52643,#52644,#52645,#52646,#52647,#52648,#52649,#52650,
#52651,#52652,#52653,#52654,#52655,#52656,#52657,#52658,#52659,#52660,#52661,
#52662,#52663,#52664,#52665,#52666,#52667,#52668,#52669,#52670,#52671,#52672,
#52673,#52674,#52675,#52676,#52677,#52678,#52679,#52680,#52681,#52682,#52683,
#52684,#52685,#52686,#52687,#52688,#52689,#52690,#52691,#52692,#52693,#52694,
#52695,#52696,#52697,#52698,#52699,#52700,#52701,#52702,#52703,#52704,#52705,
#52706,#52707,#52708,#52709,#52710,#52711,#52712,#52713,#52714,#52715,#52716,
#52717,#52718,#52719,#52720,#52721,#52722,#52723,#52724,#52725,#52726,#52727,
#52728,#52729,#52730,#52731,#52732,#52733,#52734,#52735,#52736,#52737,#52738,
#52739,#52740,#52741,#52742,#52743,#52744,#52745,#52746,#52747,#52748,#52749,
#52750,#52751,#52752,#52753,#52754,#52755,#52756,#52757,#52758,#52759,#52760,
#52761,#52762,#52763,#52764,#52765,#52766,#52767,#52768,#52769,#52770,#52771,
#52772,#52773,#52774,#52775,#52776,#52777,#52778,#52779,#52780,#52781,#52782,
#52783,#52784,#52785,#52786),.UNSPECIFIED.,.F.,.F.,(4,3,3,3,3,3,3,3,3,3,
3,3,3,3,3,3,3,3,3,3,3,3,3,3,3,3,3,3,3,3,3,3,3,3,3,3,3,3,3,3,3,3,3,3,3,3,
3,3,3,3,3,3,3,3,3,3,3,3,3,3,3,3,3,3,3,3,3,3,3,3,3,3,3,3,3,3,4),(172.78759594744,
172.87103087237,172.954453667818,173.037882341608,173.121334901619,173.204883615468,
173.288481306221,173.372218918498,173.450748875377,173.534495608079,173.618139285095,
173.701700029161,173.785197891118,173.86866039168,173.952105527173,174.035551362015,
174.119015957253,174.202569142675,174.286166976248,174.36989853911,174.449732377576,
174.533479110278,174.617122787294,174.700683531361,174.784181393318,174.86764389388,
174.951089029373,175.034534864215,175.117999459453,175.201552644875,175.285150478448,
175.36888204131,175.448715879775,175.532462612477,175.616106289493,175.699667033559,
175.783164895516,175.866627396078,175.95007253157,176.033518366413,176.116982961651,
176.200536147073,176.284133980646,176.367865543508,176.447699381975,176.531446114677,
176.615089791693,176.69865053576,176.782148397717,176.865610898279,176.949056033771,
177.032501868614,177.115966463852,177.199519649274,177.283117482847,177.366849045709,
177.446682884174,177.530429616876,177.614073293892,177.697634037959,177.781131899916,
177.864594400478,177.94803953597,178.031485370813,178.114949966051,178.198503151473,
178.282100985046,178.365832547908,178.445666386373,178.530084882565,178.614396466162,
178.698618531916,178.782768409767,178.866859317495,178.950915854996,179.034962372757,
179.07078125462),.UNSPECIFIED.);
#442=B_SPLINE_CURVE_WITH_KNOTS('',3,(#52788,#52789,#52790,#52791,#52792,
#52793,#52794,#52795,#52796,#52797,#52798,#52799,#52800,#52801,#52802,#52803,
#52804,#52805,#52806,#52807,#52808,#52809,#52810,#52811,#52812,#52813,#52814,
#52815,#52816,#52817,#52818,#52819,#52820,#52821,#52822,#52823,#52824,#52825,
#52826,#52827,#52828,#52829,#52830,#52831,#52832,#52833,#52834,#52835,#52836,
#52837,#52838,#52839,#52840,#52841,#52842,#52843,#52844,#52845,#52846,#52847,
#52848,#52849,#52850,#52851,#52852,#52853,#52854,#52855,#52856,#52857,#52858,
#52859,#52860,#52861,#52862,#52863,#52864,#52865,#52866,#52867,#52868,#52869,
#52870,#52871,#52872,#52873,#52874,#52875,#52876,#52877,#52878,#52879,#52880,
#52881,#52882,#52883,#52884,#52885,#52886,#52887,#52888,#52889,#52890,#52891,
#52892,#52893,#52894,#52895,#52896,#52897,#52898,#52899,#52900,#52901,#52902,
#52903,#52904,#52905,#52906,#52907,#52908,#52909,#52910,#52911,#52912,#52913,
#52914,#52915,#52916,#52917,#52918,#52919,#52920,#52921,#52922,#52923,#52924,
#52925,#52926,#52927,#52928,#52929,#52930,#52931,#52932,#52933,#52934,#52935,
#52936,#52937,#52938,#52939,#52940,#52941,#52942,#52943,#52944,#52945,#52946,
#52947,#52948,#52949,#52950,#52951,#52952,#52953,#52954,#52955,#52956,#52957,
#52958,#52959,#52960,#52961,#52962,#52963,#52964,#52965,#52966,#52967,#52968,
#52969,#52970,#52971,#52972,#52973,#52974,#52975,#52976,#52977,#52978,#52979,
#52980,#52981,#52982,#52983,#52984,#52985,#52986,#52987,#52988,#52989,#52990,
#52991,#52992,#52993,#52994,#52995,#52996,#52997,#52998,#52999,#53000,#53001,
#53002,#53003,#53004,#53005,#53006,#53007,#53008,#53009,#53010,#53011,#53012,
#53013),.UNSPECIFIED.,.F.,.F.,(4,3,3,3,3,3,3,3,3,3,3,3,3,3,3,3,3,3,3,3,
3,3,3,3,3,3,3,3,3,3,3,3,3,3,3,3,3,3,3,3,3,3,3,3,3,3,3,3,3,3,3,3,3,3,3,3,
3,3,3,3,3,3,3,3,3,3,3,3,3,3,3,3,3,3,3,4),(179.070781254816,179.164775236396,
179.259131704028,179.354005530881,179.444649888572,179.528396621274,179.61204029829,
179.695601042356,179.779098904313,179.862561404875,179.946006540368,180.02945237521,
180.112916970448,180.19647015587,180.280067989443,180.363799552305,180.443633390771,
180.527380123473,180.611023800489,180.694584544555,180.778082406512,180.861544907075,
180.944990042567,181.02843587741,181.111900472648,181.19545365807,181.279051491642,
181.362783054504,181.44261689297,181.526363625672,181.610007302688,181.693568046755,
181.777065908711,181.860528409274,181.943973544766,182.027419379609,182.110883974847,
182.194437160269,182.278034993842,182.361766556704,182.44160039517,182.525347127872,
182.608990804888,182.692551548954,182.776049410911,182.859511911474,182.942957046966,
183.026402881809,183.109867477047,183.193420662469,183.277018496042,183.360750058903,
183.440583897369,183.524330630071,183.607974307087,183.691535051153,183.77503291311,
183.858495413673,183.941940549165,184.025386384008,184.108850979245,184.192404164667,
184.27600199824,184.359733561102,184.439567399568,184.522368027058,184.605066337652,
184.687683334069,184.770968737519,184.853492351443,184.936002373504,185.018517639074,
185.102379869722,185.185001784602,185.269484173134,185.353966561667),
 .UNSPECIFIED.);
#443=B_SPLINE_CURVE_WITH_KNOTS('',3,(#53015,#53016,#53017,#53018,#53019,
#53020,#53021,#53022,#53023,#53024,#53025,#53026,#53027,#53028,#53029,#53030,
#53031,#53032,#53033,#53034,#53035,#53036,#53037,#53038,#53039,#53040,#53041,
#53042,#53043,#53044,#53045,#53046,#53047,#53048,#53049,#53050,#53051,#53052,
#53053,#53054,#53055,#53056,#53057,#53058,#53059,#53060,#53061,#53062,#53063,
#53064,#53065,#53066,#53067,#53068,#53069,#53070,#53071,#53072,#53073,#53074,
#53075,#53076,#53077,#53078,#53079,#53080,#53081,#53082,#53083,#53084,#53085,
#53086,#53087,#53088,#53089,#53090,#53091,#53092,#53093,#53094,#53095,#53096,
#53097,#53098,#53099,#53100,#53101,#53102,#53103,#53104,#53105,#53106,#53107,
#53108,#53109,#53110,#53111,#53112,#53113,#53114,#53115,#53116,#53117,#53118,
#53119,#53120,#53121,#53122,#53123,#53124,#53125,#53126,#53127,#53128,#53129,
#53130,#53131,#53132,#53133,#53134,#53135,#53136,#53137,#53138,#53139,#53140,
#53141,#53142,#53143,#53144,#53145,#53146,#53147,#53148,#53149,#53150,#53151,
#53152,#53153,#53154,#53155,#53156,#53157,#53158,#53159,#53160,#53161,#53162,
#53163,#53164,#53165,#53166,#53167,#53168,#53169,#53170,#53171,#53172,#53173,
#53174,#53175,#53176,#53177,#53178,#53179,#53180,#53181,#53182,#53183,#53184,
#53185,#53186,#53187,#53188,#53189,#53190,#53191,#53192,#53193,#53194,#53195,
#53196,#53197,#53198,#53199,#53200,#53201,#53202,#53203,#53204,#53205,#53206,
#53207,#53208,#53209,#53210,#53211,#53212,#53213,#53214,#53215,#53216,#53217,
#53218,#53219,#53220,#53221,#53222,#53223,#53224,#53225,#53226,#53227,#53228,
#53229,#53230,#53231,#53232,#53233,#53234,#53235,#53236,#53237,#53238,#53239,
#53240),.UNSPECIFIED.,.F.,.F.,(4,3,3,3,3,3,3,3,3,3,3,3,3,3,3,3,3,3,3,3,
3,3,3,3,3,3,3,3,3,3,3,3,3,3,3,3,3,3,3,3,3,3,3,3,3,3,3,3,3,3,3,3,3,3,3,3,
3,3,3,3,3,3,3,3,3,3,3,3,3,3,3,3,3,3,3,4),(185.353966561799,185.438550901767,
185.522297634469,185.605941311485,185.689502055551,185.772999917508,185.856462418071,
185.939907553563,186.023353388406,186.106817983644,186.190371169066,186.273969002639,
186.3577005655,186.437534403966,186.521281136668,186.604924813684,186.68848555775,
186.771983419707,186.85544592027,186.938891055762,187.022336890605,187.105801485843,
187.189354671265,187.272952504837,187.356684067699,187.436517906165,187.520264638867,
187.603908315883,187.687469059949,187.770966921906,187.854429422469,187.937874557961,
188.021320392804,188.104784988042,188.188338173464,188.271936007037,188.355667569898,
188.435501408365,188.519248141067,188.602891818083,188.686452562149,188.769950424106,
188.853412924669,188.936858060161,189.020303895004,189.103768490242,189.187321675664,
189.270919509237,189.354651072098,189.434484910564,189.518231643266,189.601875320282,
189.685436064348,189.768933926305,189.852396426867,189.935841562359,190.019287397202,
190.10275199244,190.186305177862,190.269903011434,190.353634574296,190.433468412763,
190.517215145465,190.600858822481,190.684419566548,190.767917428504,190.851379929067,
190.934825064559,191.018270899402,191.10173549464,191.185288680062,191.268886513635,
191.352618076497,191.432451914962,191.551124929453,191.637151868979),
 .UNSPECIFIED.);
#444=B_SPLINE_CURVE_WITH_KNOTS('',3,(#53242,#53243,#53244,#53245,#53246,
#53247,#53248,#53249,#53250,#53251,#53252,#53253,#53254,#53255,#53256,#53257,
#53258,#53259,#53260,#53261,#53262,#53263,#53264,#53265,#53266,#53267,#53268,
#53269,#53270,#53271,#53272,#53273,#53274,#53275,#53276,#53277,#53278,#53279,
#53280,#53281,#53282,#53283,#53284,#53285,#53286,#53287,#53288,#53289,#53290,
#53291,#53292,#53293,#53294,#53295,#53296,#53297,#53298,#53299,#53300,#53301,
#53302,#53303,#53304,#53305,#53306,#53307,#53308,#53309,#53310,#53311,#53312,
#53313,#53314,#53315,#53316,#53317,#53318,#53319,#53320,#53321,#53322,#53323,
#53324,#53325,#53326,#53327,#53328,#53329,#53330,#53331,#53332,#53333,#53334,
#53335,#53336,#53337,#53338,#53339,#53340,#53341,#53342,#53343,#53344,#53345,
#53346,#53347,#53348,#53349,#53350,#53351,#53352,#53353,#53354,#53355,#53356,
#53357,#53358,#53359,#53360,#53361,#53362,#53363,#53364,#53365,#53366,#53367,
#53368,#53369,#53370,#53371,#53372,#53373,#53374,#53375,#53376,#53377,#53378,
#53379,#53380,#53381,#53382,#53383,#53384,#53385,#53386,#53387,#53388,#53389,
#53390,#53391,#53392,#53393,#53394,#53395,#53396,#53397,#53398,#53399,#53400,
#53401,#53402,#53403,#53404,#53405,#53406,#53407,#53408,#53409,#53410,#53411,
#53412,#53413,#53414,#53415,#53416,#53417,#53418,#53419,#53420,#53421,#53422,
#53423,#53424,#53425,#53426,#53427,#53428,#53429,#53430,#53431,#53432,#53433,
#53434,#53435,#53436,#53437,#53438,#53439,#53440,#53441,#53442,#53443,#53444,
#53445,#53446,#53447,#53448,#53449,#53450,#53451,#53452,#53453,#53454,#53455,
#53456,#53457,#53458,#53459,#53460,#53461,#53462,#53463,#53464,#53465,#53466,
#53467,#53468,#53469,#53470),.UNSPECIFIED.,.F.,.F.,(4,3,3,3,3,3,3,3,3,3,
3,3,3,3,3,3,3,3,3,3,3,3,3,3,3,3,3,3,3,3,3,3,3,3,3,3,3,3,3,3,3,3,3,3,3,3,
3,3,3,3,3,3,3,3,3,3,3,3,3,3,3,3,3,3,3,3,3,3,3,3,3,3,3,3,3,3,4),(191.637151869147,
191.719547380253,191.801875435602,191.884162988348,191.966430916099,192.04869821652,
192.13098388451,192.213354359001,192.295770900865,192.37831060723,192.431435417161,
192.515182149863,192.598825826879,192.682386570945,192.765884432902,192.849346933465,
192.932792068957,193.0162379038,193.099702499038,193.18325568446,193.266853518033,
193.350585080895,193.43041891936,193.514165652062,193.597809329078,193.681370073145,
193.764867935101,193.848330435664,193.931775571156,194.015221405999,194.098686001237,
194.182239186659,194.265837020232,194.349568583093,194.429402421559,194.513149154261,
194.596792831277,194.680353575344,194.7638514373,194.847313937863,194.930759073355,
195.014204908198,195.097669503436,195.181222688858,195.264820522431,195.348552085293,
195.428385923759,195.512132656461,195.595776333477,195.679337077543,195.7628349395,
195.846297440062,195.929742575555,196.013188410397,196.096653005635,196.180206191057,
196.26380402463,196.347535587492,196.427369425958,196.51111615866,196.594759835676,
196.678320579743,196.761818441699,196.845280942262,196.928726077754,197.012171912597,
197.095636507835,197.179189693257,197.262787526829,197.346519089691,197.426352928157,
197.514630471439,197.602752823588,197.690668233066,197.778459831919,197.866087611364,
197.920337175999),.UNSPECIFIED.);
#445=B_SPLINE_CURVE_WITH_KNOTS('',3,(#53472,#53473,#53474,#53475,#53476,
#53477,#53478,#53479,#53480,#53481,#53482,#53483,#53484,#53485,#53486,#53487,
#53488,#53489,#53490,#53491,#53492,#53493,#53494,#53495,#53496,#53497,#53498,
#53499,#53500,#53501,#53502,#53503,#53504,#53505,#53506,#53507,#53508,#53509,
#53510,#53511,#53512,#53513,#53514,#53515,#53516,#53517,#53518,#53519,#53520,
#53521,#53522,#53523,#53524,#53525,#53526,#53527,#53528,#53529,#53530,#53531,
#53532,#53533,#53534,#53535,#53536,#53537,#53538,#53539,#53540,#53541,#53542,
#53543,#53544,#53545,#53546,#53547,#53548,#53549,#53550,#53551,#53552,#53553,
#53554,#53555,#53556,#53557,#53558,#53559,#53560,#53561,#53562,#53563,#53564,
#53565,#53566,#53567,#53568,#53569,#53570,#53571,#53572,#53573,#53574,#53575,
#53576,#53577,#53578,#53579,#53580,#53581,#53582,#53583,#53584,#53585,#53586,
#53587,#53588,#53589,#53590,#53591,#53592,#53593,#53594,#53595,#53596,#53597,
#53598,#53599,#53600,#53601,#53602,#53603,#53604,#53605,#53606,#53607,#53608,
#53609,#53610,#53611,#53612,#53613,#53614,#53615,#53616,#53617,#53618,#53619,
#53620,#53621,#53622,#53623,#53624,#53625,#53626,#53627,#53628,#53629,#53630,
#53631,#53632,#53633,#53634,#53635,#53636,#53637,#53638,#53639,#53640,#53641,
#53642,#53643,#53644,#53645,#53646,#53647,#53648,#53649,#53650,#53651,#53652,
#53653,#53654,#53655,#53656,#53657,#53658,#53659,#53660,#53661,#53662,#53663,
#53664,#53665,#53666,#53667,#53668,#53669,#53670,#53671,#53672,#53673,#53674,
#53675,#53676,#53677,#53678,#53679,#53680,#53681,#53682,#53683,#53684,#53685,
#53686,#53687,#53688,#53689,#53690,#53691,#53692,#53693,#53694,#53695,#53696,
#53697,#53698,#53699,#53700),.UNSPECIFIED.,.F.,.F.,(4,3,3,3,3,3,3,3,3,3,
3,3,3,3,3,3,3,3,3,3,3,3,3,3,3,3,3,3,3,3,3,3,3,3,3,3,3,3,3,3,3,3,3,3,3,3,
3,3,3,3,3,3,3,3,3,3,3,3,3,3,3,3,3,3,3,3,3,3,3,3,3,3,3,3,3,3,4),(197.920337176158,
198.007548007661,198.09486648384,198.18238412104,198.270005973806,198.357827182688,
198.425336430356,198.509083163058,198.592726840074,198.67628758414,198.759785446097,
198.843247946659,198.926693082152,199.010138916995,199.093603512233,199.177156697654,
199.260754531227,199.344486094089,199.424319932555,199.508066665257,199.591710342273,
199.675271086339,199.758768948296,199.842231448859,199.925676584351,200.009122419193,
200.092587014432,200.176140199854,200.259738033426,200.343469596288,200.423303434754,
200.507050167456,200.590693844472,200.674254588539,200.757752450496,200.841214951058,
200.924660086551,201.008105921394,201.091570516632,201.175123702054,201.258721535626,
201.342453098488,201.422286936954,201.506033669656,201.589677346672,201.673238090738,
201.756735952695,201.840198453257,201.92364358875,202.007089423592,202.09055401883,
202.174107204252,202.257705037825,202.341436600687,202.421270439153,202.505017171855,
202.588660848871,202.672221592937,202.755719454895,202.839181955457,202.92262709095,
203.006072925792,203.089537521031,203.173090706453,203.256688540026,203.340420102887,
203.420253941352,203.502850512571,203.585343452099,203.667741244618,203.750085768299,
203.832396039394,203.91469104258,203.997017564991,204.079361312531,204.161778068112,
204.203522483236),.UNSPECIFIED.);
#446=B_SPLINE_CURVE_WITH_KNOTS('',3,(#53702,#53703,#53704,#53705,#53706,
#53707,#53708,#53709,#53710,#53711,#53712,#53713,#53714,#53715,#53716,#53717,
#53718,#53719,#53720,#53721,#53722,#53723,#53724,#53725,#53726,#53727,#53728,
#53729,#53730,#53731,#53732,#53733,#53734,#53735,#53736,#53737,#53738,#53739,
#53740,#53741,#53742,#53743,#53744,#53745,#53746,#53747,#53748,#53749,#53750,
#53751,#53752,#53753,#53754,#53755,#53756,#53757,#53758,#53759,#53760,#53761,
#53762,#53763,#53764,#53765,#53766,#53767,#53768,#53769,#53770,#53771,#53772,
#53773,#53774,#53775,#53776,#53777,#53778,#53779,#53780,#53781,#53782,#53783,
#53784,#53785,#53786,#53787,#53788,#53789,#53790,#53791,#53792,#53793,#53794,
#53795,#53796,#53797,#53798,#53799,#53800,#53801,#53802,#53803,#53804,#53805,
#53806,#53807,#53808,#53809,#53810,#53811,#53812,#53813,#53814,#53815,#53816,
#53817,#53818,#53819,#53820,#53821,#53822,#53823,#53824,#53825,#53826,#53827,
#53828,#53829,#53830,#53831,#53832,#53833,#53834,#53835,#53836,#53837,#53838,
#53839,#53840,#53841,#53842,#53843,#53844,#53845,#53846,#53847,#53848,#53849,
#53850,#53851,#53852,#53853,#53854,#53855,#53856,#53857,#53858,#53859,#53860,
#53861,#53862,#53863,#53864,#53865,#53866,#53867,#53868,#53869,#53870,#53871,
#53872,#53873,#53874,#53875,#53876,#53877,#53878,#53879,#53880,#53881,#53882,
#53883,#53884,#53885,#53886,#53887,#53888,#53889,#53890,#53891,#53892,#53893,
#53894,#53895,#53896,#53897,#53898,#53899,#53900,#53901,#53902,#53903,#53904,
#53905,#53906,#53907,#53908,#53909,#53910,#53911,#53912,#53913,#53914,#53915,
#53916,#53917,#53918,#53919,#53920,#53921,#53922,#53923,#53924,#53925,#53926,
#53927),.UNSPECIFIED.,.F.,.F.,(4,3,3,3,3,3,3,3,3,3,3,3,3,3,3,3,3,3,3,3,
3,3,3,3,3,3,3,3,3,3,3,3,3,3,3,3,3,3,3,3,3,3,3,3,3,3,3,3,3,3,3,3,3,3,3,3,
3,3,3,3,3,3,3,3,3,3,3,3,3,3,3,3,3,3,3,4),(204.203522483338,204.31924029561,
204.419237443551,204.502984176253,204.586627853269,204.670188597335,204.753686459292,
204.837148959855,204.920594095347,205.00403993019,205.087504525428,205.171057710849,
205.254655544422,205.338387107284,205.41822094575,205.501967678452,205.585611355468,
205.669172099535,205.752669961491,205.836132462054,205.919577597546,206.003023432389,
206.086488027627,206.170041213049,206.253639046622,206.337370609484,206.417204447949,
206.500951180651,206.584594857667,206.668155601733,206.75165346369,206.835115964253,
206.918561099745,207.002006934588,207.085471529826,207.169024715248,207.252622548821,
207.336354111683,207.416187950149,207.499934682851,207.583578359867,207.667139103933,
207.75063696589,207.834099466453,207.917544601945,208.000990436788,208.084455032026,
208.168008217448,208.251606051021,208.335337613883,208.415171452348,208.49891818505,
208.582561862066,208.666122606132,208.749620468089,208.833082968651,208.916528104144,
208.999973938986,209.083438534224,209.166991719646,209.250589553219,209.334321116081,
209.414154954547,209.497901687249,209.581545364265,209.665106108331,209.748603970288,
209.83206647085,209.915511606343,209.998957441185,210.082422036423,210.165975221845,
210.249573055418,210.33330461828,210.413138456746,210.486707790517),
 .UNSPECIFIED.);
#447=B_SPLINE_CURVE_WITH_KNOTS('',3,(#53929,#53930,#53931,#53932,#53933,
#53934,#53935,#53936,#53937,#53938,#53939,#53940,#53941,#53942,#53943,#53944,
#53945,#53946,#53947,#53948,#53949,#53950,#53951,#53952,#53953,#53954,#53955,
#53956,#53957,#53958,#53959,#53960,#53961,#53962,#53963,#53964,#53965,#53966,
#53967,#53968,#53969,#53970,#53971,#53972,#53973,#53974,#53975,#53976,#53977,
#53978,#53979,#53980,#53981,#53982,#53983,#53984,#53985,#53986,#53987,#53988,
#53989,#53990,#53991,#53992,#53993,#53994,#53995,#53996,#53997,#53998,#53999,
#54000,#54001,#54002,#54003,#54004,#54005,#54006,#54007,#54008,#54009,#54010,
#54011,#54012,#54013,#54014,#54015,#54016,#54017,#54018,#54019,#54020,#54021,
#54022,#54023,#54024,#54025,#54026,#54027,#54028,#54029,#54030,#54031,#54032,
#54033,#54034,#54035,#54036,#54037,#54038,#54039,#54040,#54041,#54042,#54043,
#54044,#54045,#54046,#54047,#54048,#54049,#54050,#54051,#54052,#54053,#54054,
#54055,#54056,#54057,#54058,#54059,#54060,#54061,#54062,#54063,#54064,#54065,
#54066,#54067,#54068,#54069,#54070,#54071,#54072,#54073,#54074,#54075,#54076,
#54077,#54078,#54079,#54080,#54081,#54082,#54083,#54084,#54085,#54086,#54087,
#54088,#54089,#54090,#54091,#54092,#54093,#54094,#54095,#54096,#54097,#54098,
#54099,#54100,#54101,#54102,#54103,#54104,#54105,#54106,#54107,#54108,#54109,
#54110,#54111,#54112,#54113,#54114,#54115,#54116,#54117,#54118,#54119,#54120,
#54121,#54122,#54123,#54124,#54125,#54126,#54127,#54128,#54129,#54130,#54131,
#54132,#54133,#54134,#54135,#54136,#54137,#54138,#54139,#54140,#54141,#54142,
#54143,#54144,#54145,#54146,#54147,#54148,#54149,#54150,#54151,#54152,#54153,
#54154,#54155,#54156,#54157),.UNSPECIFIED.,.F.,.F.,(4,3,3,3,3,3,3,3,3,3,
3,3,3,3,3,3,3,3,3,3,3,3,3,3,3,3,3,3,3,3,3,3,3,3,3,3,3,3,3,3,3,3,3,3,3,3,
3,3,3,3,3,3,3,3,3,3,3,3,3,3,3,3,3,3,3,3,3,3,3,3,3,3,3,3,3,3,4),(210.486707790642,
210.569565422792,210.652326204392,210.735011045307,210.819649909511,210.902254524363,
210.984850690515,211.067457184152,211.15362337785,211.236351979121,211.319136610094,
211.40203416377,211.412121958945,211.495868691647,211.579512368663,211.663073112729,
211.746570974686,211.830033475249,211.913478610741,211.996924445583,212.080389040822,
212.163942226243,212.247540059816,212.331271622678,212.411105461144,212.494852193846,
212.578495870862,212.662056614928,212.745554476885,212.829016977448,212.91246211294,
212.995907947783,213.079372543021,213.162925728443,213.246523562016,213.330255124878,
213.410088963344,213.493835696046,213.577479373062,213.661040117129,213.744537979085,
213.828000479648,213.91144561514,213.994891449983,214.078356045221,214.161909230643,
214.245507064216,214.329238627077,214.409072465543,214.492819198245,214.576462875261,
214.660023619327,214.743521481284,214.826983981846,214.910429117338,214.993874952181,
215.077339547419,215.160892732841,215.244490566414,215.328222129275,215.408055967742,
215.491802700444,215.57544637746,215.659007121526,215.742504983482,215.825967484045,
215.909412619537,215.99285845438,216.076323049618,216.15987623504,216.243474068613,
216.327205631475,216.407039469941,216.502776262836,216.598179185216,216.692942127072,
216.769893097501),.UNSPECIFIED.);
#448=B_SPLINE_CURVE_WITH_KNOTS('',3,(#54159,#54160,#54161,#54162,#54163,
#54164,#54165,#54166,#54167,#54168,#54169,#54170,#54171,#54172,#54173,#54174,
#54175,#54176,#54177,#54178,#54179,#54180,#54181,#54182,#54183,#54184,#54185,
#54186,#54187,#54188,#54189,#54190,#54191,#54192,#54193,#54194,#54195,#54196,
#54197,#54198,#54199,#54200,#54201,#54202,#54203,#54204,#54205,#54206,#54207,
#54208,#54209,#54210,#54211,#54212,#54213,#54214,#54215,#54216,#54217,#54218,
#54219,#54220,#54221,#54222,#54223,#54224,#54225,#54226,#54227,#54228,#54229,
#54230,#54231,#54232,#54233,#54234,#54235,#54236,#54237,#54238,#54239,#54240,
#54241,#54242,#54243,#54244,#54245,#54246,#54247,#54248,#54249,#54250,#54251,
#54252,#54253,#54254,#54255,#54256,#54257,#54258,#54259,#54260,#54261,#54262,
#54263,#54264,#54265,#54266,#54267,#54268,#54269,#54270,#54271,#54272,#54273,
#54274,#54275,#54276,#54277,#54278,#54279,#54280,#54281,#54282,#54283,#54284,
#54285,#54286,#54287,#54288,#54289,#54290,#54291,#54292,#54293,#54294,#54295,
#54296,#54297,#54298,#54299,#54300,#54301,#54302,#54303,#54304,#54305,#54306,
#54307,#54308,#54309,#54310,#54311,#54312,#54313,#54314,#54315,#54316,#54317,
#54318,#54319,#54320,#54321,#54322,#54323,#54324,#54325,#54326,#54327,#54328,
#54329,#54330,#54331,#54332,#54333,#54334,#54335,#54336,#54337,#54338,#54339,
#54340,#54341,#54342,#54343,#54344,#54345,#54346,#54347,#54348,#54349,#54350,
#54351,#54352,#54353,#54354,#54355,#54356,#54357,#54358,#54359,#54360,#54361,
#54362,#54363,#54364,#54365,#54366,#54367,#54368,#54369,#54370,#54371,#54372,
#54373,#54374,#54375,#54376,#54377,#54378,#54379,#54380,#54381,#54382,#54383,
#54384,#54385,#54386,#54387),.UNSPECIFIED.,.F.,.F.,(4,3,3,3,3,3,3,3,3,3,
3,3,3,3,3,3,3,3,3,3,3,3,3,3,3,3,3,3,3,3,3,3,3,3,3,3,3,3,3,3,3,3,3,3,3,3,
3,3,3,3,3,3,3,3,3,3,3,3,3,3,3,3,3,3,3,3,3,3,3,3,3,3,3,3,3,3,4),(216.769893097697,
216.853753653658,216.937615196081,217.021495195232,217.105411129513,217.189432867041,
217.273513283251,217.357729007605,217.40602297214,217.489769704842,217.573413381858,
217.656974125925,217.740471987882,217.823934488444,217.907379623937,217.990825458779,
218.074290054018,218.15784323944,218.241441073012,218.325172635874,218.405006474339,
218.488753207041,218.572396884057,218.655957628123,218.73945549008,218.822917990643,
218.906363126135,218.989808960978,219.073273556216,219.156826741638,219.240424575211,
219.324156138073,219.403989976539,219.487736709241,219.571380386257,219.654941130323,
219.73843899228,219.821901492842,219.905346628335,219.988792463178,220.072257058416,
220.155810243838,220.239408077411,220.323139640272,220.402973478738,220.48672021144,
220.570363888456,220.653924632522,220.737422494479,220.820884995042,220.904330130534,
220.987775965377,221.071240560615,221.154793746037,221.238391579609,221.322123142471,
221.401956980937,221.485703713639,221.569347390655,221.652908134721,221.736405996678,
221.819868497241,221.903313632733,221.986759467576,222.070224062814,222.153777248236,
222.237375081809,222.321106644671,222.400940483136,222.484857460097,222.568672010861,
222.652402128444,222.736065743995,222.819682620366,222.903270791918,222.986866456813,
223.053078404877),.UNSPECIFIED.);
#449=B_SPLINE_CURVE_WITH_KNOTS('',3,(#54389,#54390,#54391,#54392,#54393,
#54394,#54395,#54396,#54397,#54398),.UNSPECIFIED.,.F.,.F.,(4,1,1,1,1,1,
1,4),(223.05308597169,223.399923985335,224.398907487534,225.397890989734,
226.396874491933,227.395857994132,228.394841496331,229.336256643204),
 .UNSPECIFIED.);
#450=B_SPLINE_CURVE_WITH_KNOTS('',3,(#54400,#54401,#54402,#54403,#54404,
#54405,#54406,#54407,#54408,#54409,#54410,#54411,#54412,#54413,#54414,#54415,
#54416,#54417,#54418,#54419,#54420,#54421,#54422,#54423,#54424,#54425,#54426,
#54427,#54428,#54429,#54430,#54431,#54432,#54433,#54434,#54435,#54436,#54437,
#54438,#54439,#54440,#54441,#54442,#54443,#54444,#54445,#54446,#54447,#54448,
#54449,#54450,#54451,#54452,#54453,#54454,#54455,#54456,#54457,#54458,#54459,
#54460,#54461,#54462,#54463,#54464,#54465,#54466,#54467,#54468,#54469,#54470,
#54471,#54472,#54473,#54474,#54475,#54476,#54477,#54478,#54479,#54480,#54481,
#54482,#54483,#54484,#54485,#54486,#54487,#54488,#54489,#54490,#54491,#54492,
#54493,#54494,#54495,#54496,#54497,#54498,#54499,#54500,#54501,#54502,#54503,
#54504,#54505,#54506,#54507,#54508,#54509,#54510,#54511,#54512,#54513,#54514,
#54515,#54516,#54517,#54518,#54519,#54520,#54521,#54522,#54523,#54524,#54525,
#54526,#54527,#54528,#54529,#54530,#54531,#54532,#54533,#54534,#54535,#54536,
#54537,#54538,#54539,#54540,#54541,#54542,#54543,#54544,#54545,#54546,#54547,
#54548,#54549,#54550,#54551,#54552,#54553,#54554,#54555,#54556,#54557,#54558,
#54559,#54560,#54561,#54562,#54563,#54564,#54565,#54566,#54567,#54568,#54569,
#54570,#54571,#54572,#54573,#54574,#54575,#54576,#54577,#54578,#54579,#54580,
#54581,#54582,#54583,#54584,#54585,#54586,#54587,#54588,#54589,#54590,#54591,
#54592,#54593,#54594,#54595,#54596,#54597,#54598,#54599,#54600,#54601,#54602,
#54603,#54604,#54605,#54606,#54607,#54608,#54609,#54610,#54611,#54612,#54613,
#54614,#54615,#54616,#54617,#54618,#54619,#54620,#54621,#54622,#54623,#54624,
#54625),.UNSPECIFIED.,.F.,.F.,(4,3,3,3,3,3,3,3,3,3,3,3,3,3,3,3,3,3,3,3,
3,3,3,3,3,3,3,3,3,3,3,3,3,3,3,3,3,3,3,3,3,3,3,3,3,3,3,3,3,3,3,3,3,3,3,3,
3,3,3,3,3,3,3,3,3,3,3,3,3,3,3,3,3,3,3,4),(229.336263712056,229.39382499853,
229.477571731232,229.561215408248,229.644776152314,229.728274014271,229.811736514833,
229.895181650326,229.978627485168,230.062092080407,230.145645265828,230.229243099401,
230.312974662263,230.392808500729,230.476555233431,230.560198910447,230.643759654514,
230.72725751647,230.810720017033,230.894165152525,230.977610987368,231.061075582606,
231.144628768028,231.228226601601,231.311958164463,231.391792002929,231.475538735631,
231.559182412647,231.642743156713,231.72624101867,231.809703519233,231.893148654725,
231.976594489568,232.060059084806,232.143612270228,232.2272101038,232.310941666662,
232.390775505128,232.47452223783,232.558165914846,232.641726658912,232.725224520869,
232.808687021432,232.892132156924,232.975577991767,233.059042587005,233.142595772427,
233.226193605999,233.309925168861,233.389759007327,233.473505740029,233.557149417045,
233.640710161111,233.724208023068,233.80767052363,233.891115659123,233.974561493965,
234.058026089203,234.141579274625,234.225177108198,234.30890867106,234.388742509526,
234.472489242228,234.556132919244,234.63969366331,234.723191525267,234.80665402583,
234.890099161322,234.973544996165,235.057009591403,235.140562776825,235.224160610397,
235.307892173259,235.387726011725,235.50358751548,235.619449019236),
 .UNSPECIFIED.);
#451=B_SPLINE_CURVE_WITH_KNOTS('',3,(#54627,#54628,#54629,#54630,#54631,
#54632,#54633,#54634,#54635,#54636,#54637,#54638,#54639,#54640,#54641,#54642,
#54643,#54644,#54645,#54646,#54647,#54648,#54649,#54650,#54651,#54652,#54653,
#54654,#54655,#54656,#54657,#54658,#54659,#54660,#54661,#54662,#54663,#54664,
#54665,#54666,#54667,#54668,#54669,#54670,#54671,#54672,#54673,#54674,#54675,
#54676,#54677,#54678,#54679,#54680,#54681,#54682,#54683,#54684,#54685,#54686,
#54687,#54688,#54689,#54690,#54691,#54692,#54693,#54694,#54695,#54696,#54697,
#54698,#54699,#54700,#54701,#54702,#54703,#54704,#54705,#54706,#54707,#54708,
#54709,#54710,#54711,#54712,#54713,#54714,#54715,#54716,#54717,#54718,#54719,
#54720,#54721,#54722,#54723,#54724,#54725,#54726,#54727,#54728,#54729,#54730,
#54731,#54732,#54733,#54734,#54735,#54736,#54737,#54738,#54739,#54740,#54741,
#54742,#54743,#54744,#54745,#54746,#54747,#54748,#54749,#54750,#54751,#54752,
#54753,#54754,#54755,#54756,#54757,#54758,#54759,#54760,#54761,#54762,#54763,
#54764,#54765,#54766,#54767,#54768,#54769,#54770,#54771,#54772,#54773,#54774,
#54775,#54776,#54777,#54778,#54779,#54780,#54781,#54782,#54783,#54784,#54785,
#54786,#54787,#54788,#54789,#54790,#54791,#54792,#54793,#54794,#54795,#54796,
#54797,#54798,#54799,#54800,#54801,#54802,#54803,#54804,#54805,#54806,#54807,
#54808,#54809,#54810,#54811,#54812,#54813,#54814,#54815,#54816,#54817,#54818,
#54819,#54820,#54821,#54822,#54823,#54824,#54825,#54826,#54827,#54828,#54829,
#54830,#54831,#54832,#54833,#54834,#54835,#54836,#54837,#54838,#54839,#54840,
#54841,#54842,#54843,#54844,#54845,#54846,#54847,#54848,#54849,#54850,#54851,
#54852,#54853,#54854,#54855),.UNSPECIFIED.,.F.,.F.,(4,3,3,3,3,3,3,3,3,3,
3,3,3,3,3,3,3,3,3,3,3,3,3,3,3,3,3,3,3,3,3,3,3,3,3,3,3,3,3,3,3,3,3,3,3,3,
3,3,3,3,3,3,3,3,3,3,3,3,3,3,3,3,3,3,3,3,3,3,3,3,3,3,3,3,3,3,4),(235.619449019367,
235.701928974608,235.787526542023,235.869916952055,235.952295875165,236.034682232197,
236.117094947374,236.199596927949,236.282152013071,236.364822636091,236.386709513924,
236.470456246626,236.554099923642,236.637660667708,236.721158529665,236.804621030228,
236.88806616572,236.971512000563,237.054976595801,237.138529781223,237.222127614796,
237.305859177658,237.385693016124,237.469439748826,237.553083425842,237.636644169909,
237.720142031865,237.803604532428,237.88704966792,237.970495502763,238.053960098001,
238.137513283423,238.221111116996,238.304842679858,238.384676518323,238.468423251025,
238.552066928041,238.635627672107,238.719125534064,238.802588034626,238.886033170119,
238.969479004961,239.0529436002,239.136496785621,239.220094619194,239.303826182056,
239.383660020522,239.467406753224,239.55105043024,239.634611174306,239.718109036263,
239.801571536825,239.885016672318,239.968462507161,240.051927102398,240.13548028782,
240.219078121393,240.302809684255,240.382643522721,240.466390255423,240.550033932439,
240.633594676506,240.717092538462,240.800555039025,240.884000174517,240.96744600936,
241.050910604598,241.13446379002,241.218061623593,241.301793186454,241.38162702492,
241.468881254052,241.555995737591,241.642932265323,241.729764964557,241.816468207509,
241.902634326415),.UNSPECIFIED.);
#452=B_SPLINE_CURVE_WITH_KNOTS('',3,(#54857,#54858,#54859,#54860,#54861,
#54862,#54863,#54864,#54865,#54866,#54867,#54868,#54869,#54870,#54871,#54872,
#54873,#54874,#54875,#54876,#54877,#54878,#54879,#54880,#54881,#54882,#54883,
#54884,#54885,#54886,#54887,#54888,#54889,#54890,#54891,#54892,#54893,#54894,
#54895,#54896,#54897,#54898,#54899,#54900,#54901,#54902,#54903,#54904,#54905,
#54906,#54907,#54908,#54909,#54910,#54911,#54912,#54913,#54914,#54915,#54916,
#54917,#54918,#54919,#54920,#54921,#54922,#54923,#54924,#54925,#54926,#54927,
#54928,#54929,#54930,#54931,#54932,#54933,#54934,#54935,#54936,#54937,#54938,
#54939,#54940,#54941,#54942,#54943,#54944,#54945,#54946,#54947,#54948,#54949,
#54950,#54951,#54952,#54953,#54954,#54955,#54956,#54957,#54958,#54959,#54960,
#54961,#54962,#54963,#54964,#54965,#54966,#54967,#54968,#54969,#54970,#54971,
#54972,#54973,#54974,#54975,#54976,#54977,#54978,#54979,#54980,#54981,#54982,
#54983,#54984,#54985,#54986,#54987,#54988,#54989,#54990,#54991,#54992,#54993,
#54994,#54995,#54996,#54997,#54998,#54999,#55000,#55001,#55002,#55003,#55004,
#55005,#55006,#55007,#55008,#55009,#55010,#55011,#55012,#55013,#55014,#55015,
#55016,#55017,#55018,#55019,#55020,#55021,#55022,#55023,#55024,#55025,#55026,
#55027,#55028,#55029,#55030,#55031,#55032,#55033,#55034,#55035,#55036,#55037,
#55038,#55039,#55040,#55041,#55042,#55043,#55044,#55045,#55046,#55047,#55048,
#55049,#55050,#55051,#55052,#55053,#55054,#55055,#55056,#55057,#55058,#55059,
#55060,#55061,#55062,#55063,#55064,#55065,#55066,#55067,#55068,#55069,#55070,
#55071,#55072,#55073,#55074,#55075,#55076,#55077,#55078,#55079,#55080,#55081,
#55082,#55083,#55084,#55085),.UNSPECIFIED.,.F.,.F.,(4,3,3,3,3,3,3,3,3,3,
3,3,3,3,3,3,3,3,3,3,3,3,3,3,3,3,3,3,3,3,3,3,3,3,3,3,3,3,3,3,3,3,3,3,3,3,
3,3,3,3,3,3,3,3,3,3,3,3,3,3,3,3,3,3,3,3,3,3,3,3,3,3,3,3,3,3,4),(241.902634326614,
241.990863900032,242.079239902703,242.167853017759,242.256595129932,242.345544125978,
242.380610527119,242.464357259821,242.548000936837,242.631561680904,242.71505954286,
242.798522043423,242.881967178915,242.965413013758,243.048877608996,243.132430794418,
243.216028627991,243.299760190852,243.379594029319,243.463340762021,243.546984439037,
243.630545183103,243.71404304506,243.797505545623,243.880950681115,243.964396515958,
244.047861111196,244.131414296618,244.21501213019,244.298743693052,244.378577531518,
244.46232426422,244.545967941236,244.629528685302,244.713026547259,244.796489047822,
244.879934183314,244.963380018157,245.046844613395,245.130397798817,245.213995632389,
245.297727195251,245.377561033717,245.461307766419,245.544951443435,245.628512187501,
245.712010049458,245.795472550021,245.878917685513,245.962363520356,246.045828115594,
246.129381301015,246.212979134588,246.29671069745,246.376544535916,246.460291268618,
246.543934945634,246.6274956897,246.710993551657,246.79445605222,246.877901187712,
246.961347022555,247.044811617793,247.128364803215,247.211962636788,247.295694199649,
247.375528038115,247.458043982855,247.54045702969,247.622776737558,247.705044162818,
247.787278368309,247.869498385905,247.951756669092,248.034032929656,248.116396974214,
248.185819633464),.UNSPECIFIED.);
#453=B_SPLINE_CURVE_WITH_KNOTS('',3,(#55087,#55088,#55089,#55090,#55091,
#55092,#55093,#55094,#55095,#55096,#55097,#55098,#55099,#55100,#55101,#55102,
#55103,#55104,#55105,#55106,#55107,#55108,#55109,#55110,#55111,#55112,#55113,
#55114,#55115,#55116,#55117,#55118,#55119,#55120,#55121,#55122,#55123,#55124,
#55125,#55126,#55127,#55128,#55129,#55130,#55131,#55132,#55133,#55134,#55135,
#55136,#55137,#55138,#55139,#55140,#55141,#55142,#55143,#55144,#55145,#55146,
#55147,#55148,#55149,#55150,#55151,#55152,#55153,#55154,#55155,#55156,#55157,
#55158,#55159,#55160,#55161,#55162,#55163,#55164,#55165,#55166,#55167,#55168,
#55169,#55170,#55171,#55172,#55173,#55174,#55175,#55176,#55177,#55178,#55179,
#55180,#55181,#55182,#55183,#55184,#55185,#55186,#55187,#55188,#55189,#55190,
#55191,#55192,#55193,#55194,#55195,#55196,#55197,#55198,#55199,#55200,#55201,
#55202,#55203,#55204,#55205,#55206,#55207,#55208,#55209,#55210,#55211,#55212,
#55213,#55214,#55215,#55216,#55217,#55218,#55219,#55220,#55221,#55222,#55223,
#55224,#55225,#55226,#55227,#55228,#55229,#55230,#55231,#55232,#55233,#55234,
#55235,#55236,#55237,#55238,#55239,#55240,#55241,#55242,#55243,#55244,#55245,
#55246,#55247,#55248,#55249,#55250,#55251,#55252,#55253,#55254,#55255,#55256,
#55257,#55258,#55259,#55260,#55261,#55262,#55263,#55264,#55265,#55266,#55267,
#55268,#55269,#55270,#55271,#55272,#55273,#55274,#55275,#55276,#55277,#55278,
#55279,#55280,#55281,#55282,#55283,#55284,#55285,#55286,#55287,#55288,#55289,
#55290,#55291,#55292,#55293,#55294,#55295,#55296,#55297,#55298,#55299,#55300,
#55301,#55302,#55303,#55304,#55305,#55306,#55307,#55308,#55309,#55310,#55311,
#55312),.UNSPECIFIED.,.F.,.F.,(4,3,3,3,3,3,3,3,3,3,3,3,3,3,3,3,3,3,3,3,
3,3,3,3,3,3,3,3,3,3,3,3,3,3,3,3,3,3,3,3,3,3,3,3,3,3,3,3,3,3,3,3,3,3,3,3,
3,3,3,3,3,3,3,3,3,3,3,3,3,3,3,3,3,3,3,4),(248.185819633595,248.309579357114,
248.374511540314,248.458258273016,248.541901950032,248.625462694098,248.708960556055,
248.792423056618,248.87586819211,248.959314026953,249.042778622192,249.126331807613,
249.209929641186,249.293661204048,249.373495042514,249.457241775216,249.540885452232,
249.624446196298,249.707944058255,249.791406558818,249.87485169431,249.958297529153,
250.041762124391,250.125315309813,250.208913143386,250.292644706248,250.372478544713,
250.456225277415,250.539868954431,250.623429698497,250.706927560454,250.790390061016,
250.873835196508,250.957281031351,251.040745626589,251.124298812011,251.207896645583,
251.291628208445,251.371462046912,251.455208779614,251.53885245663,251.622413200696,
251.705911062653,251.789373563216,251.872818698708,251.956264533551,252.039729128789,
252.123282314211,252.206880147784,252.290611710646,252.370445549111,252.454192281813,
252.537835958829,252.621396702895,252.704894564852,252.788357065414,252.871802200907,
252.955248035749,253.038712630987,253.122265816409,253.205863649982,253.289595212844,
253.36942905131,253.453175784012,253.536819461028,253.620380205095,253.703878067051,
253.787340567614,253.870785703106,253.954231537949,254.037696133187,254.121249318609,
254.204847152182,254.288578715044,254.368412553509,254.469004940774),
 .UNSPECIFIED.);
#454=B_SPLINE_CURVE_WITH_KNOTS('',3,(#55314,#55315,#55316,#55317,#55318,
#55319,#55320,#55321,#55322,#55323,#55324,#55325,#55326,#55327,#55328,#55329,
#55330,#55331,#55332,#55333,#55334,#55335,#55336,#55337,#55338,#55339,#55340,
#55341,#55342,#55343,#55344,#55345,#55346,#55347,#55348,#55349,#55350,#55351,
#55352,#55353,#55354,#55355,#55356,#55357,#55358,#55359,#55360,#55361,#55362,
#55363,#55364,#55365,#55366,#55367,#55368,#55369,#55370,#55371,#55372,#55373,
#55374,#55375,#55376,#55377,#55378,#55379,#55380,#55381,#55382,#55383,#55384,
#55385,#55386,#55387,#55388,#55389,#55390,#55391,#55392,#55393,#55394,#55395,
#55396,#55397,#55398,#55399,#55400,#55401,#55402,#55403,#55404,#55405,#55406,
#55407,#55408,#55409,#55410,#55411,#55412,#55413,#55414,#55415,#55416,#55417,
#55418,#55419,#55420,#55421,#55422,#55423,#55424,#55425,#55426,#55427,#55428,
#55429,#55430,#55431,#55432,#55433,#55434,#55435,#55436,#55437,#55438,#55439,
#55440,#55441,#55442,#55443,#55444,#55445,#55446,#55447,#55448,#55449,#55450,
#55451,#55452,#55453,#55454,#55455,#55456,#55457,#55458,#55459,#55460,#55461,
#55462,#55463,#55464,#55465,#55466,#55467,#55468,#55469,#55470,#55471,#55472,
#55473,#55474,#55475,#55476,#55477,#55478,#55479,#55480,#55481,#55482,#55483,
#55484,#55485,#55486,#55487,#55488,#55489,#55490,#55491,#55492,#55493,#55494,
#55495,#55496,#55497,#55498,#55499,#55500,#55501,#55502,#55503,#55504,#55505,
#55506,#55507,#55508,#55509,#55510,#55511,#55512,#55513,#55514,#55515,#55516,
#55517,#55518,#55519,#55520,#55521,#55522,#55523,#55524,#55525,#55526,#55527,
#55528,#55529,#55530,#55531,#55532,#55533,#55534,#55535,#55536,#55537,#55538,
#55539,#55540,#55541,#55542),.UNSPECIFIED.,.F.,.F.,(4,3,3,3,3,3,3,3,3,3,
3,3,3,3,3,3,3,3,3,3,3,3,3,3,3,3,3,3,3,3,3,3,3,3,3,3,3,3,3,3,3,3,3,3,3,3,
3,3,3,3,3,3,3,3,3,3,3,3,3,3,3,3,3,3,3,3,3,3,3,3,3,3,3,3,3,3,4),(254.469004940909,
254.551650520092,254.634203710762,254.716685552544,254.799121637284,254.881534416937,
254.96394280165,255.046365695572,255.128871881607,255.211420494891,255.294098388882,
255.367396055709,255.451142788411,255.534786465427,255.618347209493,255.70184507145,
255.785307572013,255.868752707505,255.952198542348,256.035663137586,256.119216323008,
256.202814156581,256.286545719443,256.366379557908,256.45012629061,256.533769967626,
256.617330711692,256.700828573648,256.784291074211,256.867736209703,256.951182044546,
257.034646639784,257.118199825206,257.201797658778,257.28552922164,257.365363060107,
257.449109792809,257.532753469825,257.616314213891,257.699812075848,257.783274576411,
257.866719711903,257.950165546746,258.033630141984,258.117183327406,258.200781160979,
258.284512723841,258.364346562306,258.448093295008,258.531736972024,258.61529771609,
258.698795578046,258.782258078609,258.865703214101,258.949149048944,259.032613644182,
259.116166829604,259.199764663176,259.283496226038,259.363330064505,259.447076797207,
259.530720474223,259.614281218289,259.697779080246,259.781241580809,259.864686716301,
259.948132551144,260.031597146382,260.115150331804,260.198748165377,260.282479728238,
260.362313566704,260.45978273697,260.553217387915,260.646361478217,260.73906526939,
260.752190247769),.UNSPECIFIED.);
#455=B_SPLINE_CURVE_WITH_KNOTS('',3,(#55544,#55545,#55546,#55547,#55548,
#55549,#55550,#55551,#55552,#55553,#55554,#55555,#55556,#55557,#55558,#55559,
#55560,#55561,#55562,#55563,#55564,#55565,#55566,#55567,#55568,#55569,#55570,
#55571,#55572,#55573,#55574,#55575,#55576,#55577,#55578,#55579,#55580,#55581,
#55582,#55583,#55584,#55585,#55586,#55587,#55588,#55589,#55590,#55591,#55592,
#55593,#55594,#55595,#55596,#55597,#55598,#55599,#55600,#55601,#55602,#55603,
#55604,#55605,#55606,#55607,#55608,#55609,#55610,#55611,#55612,#55613,#55614,
#55615,#55616,#55617,#55618,#55619,#55620,#55621,#55622,#55623,#55624,#55625,
#55626,#55627,#55628,#55629,#55630,#55631,#55632,#55633,#55634,#55635,#55636,
#55637,#55638,#55639,#55640,#55641,#55642,#55643,#55644,#55645,#55646,#55647,
#55648,#55649,#55650,#55651,#55652,#55653,#55654,#55655,#55656,#55657,#55658,
#55659,#55660,#55661,#55662,#55663,#55664,#55665,#55666,#55667,#55668,#55669,
#55670,#55671,#55672,#55673,#55674,#55675,#55676,#55677,#55678,#55679,#55680,
#55681,#55682,#55683,#55684,#55685,#55686,#55687,#55688,#55689,#55690,#55691,
#55692,#55693,#55694,#55695,#55696,#55697,#55698,#55699,#55700,#55701,#55702,
#55703,#55704,#55705,#55706,#55707,#55708,#55709,#55710,#55711,#55712,#55713,
#55714,#55715,#55716,#55717,#55718,#55719,#55720,#55721,#55722,#55723,#55724,
#55725,#55726,#55727,#55728,#55729,#55730,#55731,#55732,#55733,#55734,#55735,
#55736,#55737,#55738,#55739,#55740,#55741,#55742,#55743,#55744,#55745,#55746,
#55747,#55748,#55749,#55750,#55751,#55752,#55753,#55754,#55755,#55756,#55757,
#55758,#55759,#55760,#55761,#55762,#55763,#55764,#55765,#55766,#55767,#55768,
#55769,#55770,#55771,#55772),.UNSPECIFIED.,.F.,.F.,(4,3,3,3,3,3,3,3,3,3,
3,3,3,3,3,3,3,3,3,3,3,3,3,3,3,3,3,3,3,3,3,3,3,3,3,3,3,3,3,3,3,3,3,3,3,3,
3,3,3,3,3,3,3,3,3,3,3,3,3,3,3,3,3,3,3,3,3,3,3,3,3,3,3,3,3,3,4),(260.752190247954,
260.836557566651,260.920941027191,261.005357334773,261.08982321306,261.174405754682,
261.259057630092,261.343841100169,261.361297068904,261.445043801606,261.528687478622,
261.612248222688,261.695746084645,261.779208585207,261.8626537207,261.946099555542,
262.02956415078,262.113117336202,262.196715169775,262.280446732637,262.360280571103,
262.444027303805,262.527670980821,262.611231724887,262.694729586844,262.778192087407,
262.861637222899,262.945083057742,263.02854765298,263.112100838401,263.195698671974,
263.279430234836,263.359264073302,263.443010806004,263.52665448302,263.610215227086,
263.693713089043,263.777175589605,263.860620725097,263.94406655994,264.027531155178,
264.1110843406,264.194682174172,264.278413737034,264.358247575501,264.441994308203,
264.525637985219,264.609198729286,264.692696591243,264.776159091805,264.859604227298,
264.943050062141,265.026514657379,265.110067842801,265.193665676373,265.277397239235,
265.3572310777,265.440977810402,265.524621487418,265.608182231484,265.691680093441,
265.775142594003,265.858587729496,265.942033564339,266.025498159577,266.109051344999,
266.192649178571,266.276380741433,266.356214579899,266.441109701803,266.524506460389,
266.607823017449,266.69107772501,266.777152182541,266.860346617411,266.947861086272,
267.035375555133),.UNSPECIFIED.);
#456=B_SPLINE_CURVE_WITH_KNOTS('',3,(#55774,#55775,#55776,#55777,#55778,
#55779,#55780,#55781,#55782,#55783,#55784,#55785,#55786,#55787,#55788,#55789,
#55790,#55791,#55792,#55793,#55794,#55795,#55796,#55797,#55798,#55799,#55800,
#55801,#55802,#55803,#55804,#55805,#55806,#55807,#55808,#55809,#55810,#55811,
#55812,#55813,#55814,#55815,#55816,#55817,#55818,#55819,#55820,#55821,#55822,
#55823,#55824,#55825,#55826,#55827,#55828,#55829,#55830,#55831,#55832,#55833,
#55834,#55835,#55836,#55837,#55838,#55839,#55840,#55841,#55842,#55843,#55844,
#55845,#55846,#55847,#55848,#55849,#55850,#55851,#55852,#55853,#55854,#55855,
#55856,#55857,#55858,#55859,#55860,#55861,#55862,#55863,#55864,#55865,#55866,
#55867,#55868,#55869,#55870,#55871,#55872,#55873,#55874,#55875,#55876,#55877,
#55878,#55879,#55880,#55881,#55882,#55883,#55884,#55885,#55886,#55887,#55888,
#55889,#55890,#55891,#55892,#55893,#55894,#55895,#55896,#55897,#55898,#55899,
#55900,#55901,#55902,#55903,#55904,#55905,#55906,#55907,#55908,#55909,#55910,
#55911,#55912,#55913,#55914,#55915,#55916,#55917,#55918,#55919,#55920,#55921,
#55922,#55923,#55924,#55925,#55926,#55927,#55928,#55929,#55930,#55931,#55932,
#55933,#55934,#55935,#55936,#55937,#55938,#55939,#55940,#55941,#55942,#55943,
#55944,#55945,#55946,#55947,#55948,#55949,#55950,#55951,#55952,#55953,#55954,
#55955,#55956,#55957,#55958,#55959,#55960,#55961,#55962,#55963,#55964,#55965,
#55966,#55967,#55968,#55969,#55970,#55971,#55972,#55973,#55974,#55975,#55976,
#55977,#55978,#55979,#55980,#55981,#55982,#55983,#55984,#55985,#55986,#55987,
#55988,#55989,#55990,#55991,#55992,#55993,#55994,#55995,#55996,#55997,#55998,
#55999,#56000,#56001,#56002),.UNSPECIFIED.,.F.,.F.,(4,3,3,3,3,3,3,3,3,3,
3,3,3,3,3,3,3,3,3,3,3,3,3,3,3,3,3,3,3,3,3,3,3,3,3,3,3,3,3,3,3,3,3,3,3,3,
3,3,3,3,3,3,3,3,3,3,3,3,3,3,3,3,3,3,3,3,3,3,3,3,3,3,3,3,3,3,4),(267.035375555307,
267.13383122682,267.232963513412,267.332840407885,267.355198082099,267.438944814801,
267.522588491817,267.606149235883,267.68964709784,267.773109598403,267.856554733895,
267.940000568738,268.023465163976,268.107018349398,268.19061618297,268.274347745832,
268.354181584298,268.437928317,268.521571994016,268.605132738082,268.688630600039,
268.772093100602,268.855538236094,268.938984070937,269.022448666175,269.106001851597,
269.189599685169,269.273331248031,269.353165086497,269.436911819199,269.520555496215,
269.604116240281,269.687614102238,269.7710766028,269.854521738292,269.937967573135,
270.021432168373,270.104985353795,270.188583187367,270.272314750229,270.352148588696,
270.435895321398,270.519538998414,270.60309974248,270.686597604437,270.770060105,
270.853505240492,270.936951075335,271.020415670573,271.103968855995,271.187566689568,
271.27129825243,271.351132090895,271.434878823597,271.518522500613,271.602083244679,
271.685581106636,271.769043607199,271.852488742691,271.935934577534,272.019399172772,
272.102952358194,272.186550191766,272.270281754628,272.350115593094,272.433442907024,
272.516667437266,272.599809733204,272.682890268008,272.765937076089,272.848968279795,
272.932002321396,273.015057641556,273.098200588014,273.181391202307,273.264706059386,
273.318560584361),.UNSPECIFIED.);
#457=B_SPLINE_CURVE_WITH_KNOTS('',3,(#56004,#56005,#56006,#56007,#56008,
#56009,#56010,#56011,#56012,#56013,#56014),.UNSPECIFIED.,.F.,.F.,(4,1,1,
1,1,1,1,1,4),(273.318560862313,273.349099095293,274.348082597493,275.347066099692,
276.346049601891,277.34503310409,278.344016606289,279.343000108488,279.60174364527),
 .UNSPECIFIED.);
#458=B_SPLINE_CURVE_WITH_KNOTS('',3,(#56016,#56017,#56018,#56019,#56020,
#56021,#56022,#56023,#56024,#56025,#56026,#56027,#56028,#56029,#56030,#56031,
#56032,#56033,#56034,#56035,#56036,#56037,#56038,#56039,#56040,#56041,#56042,
#56043,#56044,#56045,#56046,#56047,#56048,#56049,#56050,#56051,#56052,#56053,
#56054,#56055,#56056,#56057,#56058,#56059,#56060,#56061,#56062,#56063,#56064,
#56065,#56066,#56067,#56068,#56069,#56070,#56071,#56072,#56073,#56074,#56075,
#56076,#56077,#56078,#56079,#56080,#56081,#56082,#56083,#56084,#56085,#56086,
#56087,#56088,#56089,#56090,#56091,#56092,#56093,#56094,#56095,#56096,#56097,
#56098,#56099,#56100,#56101,#56102,#56103,#56104,#56105,#56106,#56107,#56108,
#56109,#56110,#56111,#56112,#56113,#56114,#56115,#56116,#56117,#56118,#56119,
#56120,#56121,#56122,#56123,#56124,#56125,#56126,#56127,#56128,#56129,#56130,
#56131,#56132,#56133,#56134,#56135,#56136,#56137,#56138,#56139,#56140,#56141,
#56142,#56143,#56144,#56145,#56146,#56147,#56148,#56149,#56150,#56151,#56152,
#56153,#56154,#56155,#56156,#56157,#56158,#56159,#56160,#56161,#56162,#56163,
#56164,#56165,#56166,#56167,#56168,#56169,#56170,#56171,#56172,#56173,#56174,
#56175,#56176,#56177,#56178,#56179,#56180,#56181,#56182,#56183,#56184,#56185,
#56186,#56187,#56188,#56189,#56190,#56191,#56192,#56193,#56194,#56195,#56196,
#56197,#56198,#56199,#56200,#56201,#56202,#56203,#56204,#56205,#56206,#56207,
#56208,#56209,#56210,#56211,#56212,#56213,#56214,#56215,#56216,#56217,#56218,
#56219,#56220,#56221,#56222,#56223,#56224,#56225,#56226,#56227,#56228,#56229,
#56230,#56231,#56232,#56233,#56234,#56235,#56236,#56237,#56238,#56239,#56240,
#56241,#56242,#56243,#56244),.UNSPECIFIED.,.F.,.F.,(4,3,3,3,3,3,3,3,3,3,
3,3,3,3,3,3,3,3,3,3,3,3,3,3,3,3,3,3,3,3,3,3,3,3,3,3,3,3,3,3,3,3,3,3,3,3,
3,3,3,3,3,3,3,3,3,3,3,3,3,3,3,3,3,3,3,3,3,3,3,3,3,3,3,3,3,3,4),(279.601746169493,
279.684374539858,279.766958048281,279.849518653294,279.932075157065,280.014646355849,
280.097302135208,280.180000280235,280.262830816679,280.341983610688,280.42573034339,
280.509374020406,280.592934764472,280.676432626429,280.759895126992,280.843340262484,
280.926786097327,281.010250692565,281.093803877987,281.177401711559,281.261133274421,
281.340967112887,281.424713845589,281.508357522604,281.591918266671,281.675416128628,
281.75887862919,281.842323764683,281.925769599525,282.009234194764,282.092787380185,
282.176385213758,282.26011677662,282.339950615086,282.423697347788,282.507341024804,
282.590901768871,282.674399630827,282.75786213139,282.841307266882,282.924753101725,
283.008217696963,283.091770882385,283.175368715958,283.25910027882,283.338934117285,
283.422680849987,283.506324527003,283.589885271069,283.673383133026,283.756845633589,
283.840290769081,283.923736603923,284.007201199161,284.090754384583,284.174352218155,
284.258083781017,284.337917619484,284.421664352186,284.505308029202,284.588868773268,
284.672366635225,284.755829135787,284.83927427128,284.922720106122,285.00618470136,
285.089737886782,285.173335720355,285.257067283217,285.336901121683,285.423263322375,
285.509497592493,285.595617755227,285.681608329013,285.767522176602,285.853356753516,
285.884931476672),.UNSPECIFIED.);
#459=B_SPLINE_CURVE_WITH_KNOTS('',3,(#56246,#56247,#56248,#56249,#56250,
#56251,#56252,#56253,#56254,#56255,#56256,#56257,#56258,#56259,#56260,#56261,
#56262,#56263,#56264,#56265,#56266,#56267,#56268,#56269,#56270,#56271,#56272,
#56273,#56274,#56275,#56276,#56277,#56278,#56279,#56280,#56281,#56282,#56283,
#56284,#56285,#56286,#56287,#56288,#56289,#56290,#56291,#56292,#56293,#56294,
#56295,#56296,#56297,#56298,#56299,#56300,#56301,#56302,#56303,#56304,#56305,
#56306,#56307,#56308,#56309,#56310,#56311,#56312,#56313,#56314,#56315,#56316,
#56317,#56318,#56319,#56320,#56321,#56322,#56323,#56324,#56325,#56326,#56327,
#56328,#56329,#56330,#56331,#56332,#56333,#56334,#56335,#56336,#56337,#56338,
#56339,#56340,#56341,#56342,#56343,#56344,#56345,#56346,#56347,#56348,#56349,
#56350,#56351,#56352,#56353,#56354,#56355,#56356,#56357,#56358,#56359,#56360,
#56361,#56362,#56363,#56364,#56365,#56366,#56367,#56368,#56369,#56370,#56371,
#56372,#56373,#56374,#56375,#56376,#56377,#56378,#56379,#56380,#56381,#56382,
#56383,#56384,#56385,#56386,#56387,#56388,#56389,#56390,#56391,#56392,#56393,
#56394,#56395,#56396,#56397,#56398,#56399,#56400,#56401,#56402,#56403,#56404,
#56405,#56406,#56407,#56408,#56409,#56410,#56411,#56412,#56413,#56414,#56415,
#56416,#56417,#56418,#56419,#56420,#56421,#56422,#56423,#56424,#56425,#56426,
#56427,#56428,#56429,#56430,#56431,#56432,#56433,#56434,#56435,#56436,#56437,
#56438,#56439,#56440,#56441,#56442,#56443,#56444,#56445,#56446,#56447,#56448,
#56449,#56450,#56451,#56452,#56453,#56454,#56455,#56456,#56457,#56458,#56459,
#56460,#56461,#56462,#56463,#56464,#56465,#56466,#56467,#56468,#56469,#56470,
#56471,#56472,#56473,#56474),.UNSPECIFIED.,.F.,.F.,(4,3,3,3,3,3,3,3,3,3,
3,3,3,3,3,3,3,3,3,3,3,3,3,3,3,3,3,3,3,3,3,3,3,3,3,3,3,3,3,3,3,3,3,3,3,3,
3,3,3,3,3,3,3,3,3,3,3,3,3,3,3,3,3,3,3,3,3,3,3,3,3,3,3,3,3,3,4),(285.884931476777,
285.974324781646,286.064714742205,286.154589823141,286.245237223512,286.335884623883,
286.419631356585,286.503275033601,286.586835777667,286.670333639624,286.753796140187,
286.837241275679,286.920687110522,287.00415170576,287.087704891182,287.171302724755,
287.255034287617,287.334868126082,287.418614858784,287.5022585358,287.585819279866,
287.669317141823,287.752779642385,287.836224777877,287.91967061272,288.003135207958,
288.08668839338,288.170286226953,288.254017789814,288.333851628281,288.417598360983,
288.501242037999,288.584802782065,288.668300644022,288.751763144585,288.835208280077,
288.91865411492,289.002118710158,289.08567189558,289.169269729153,289.253001292015,
289.33283513048,289.416581863182,289.500225540198,289.583786284264,289.667284146221,
289.750746646783,289.834191782276,289.917637617118,290.001102212356,290.084655397778,
290.168253231351,290.251984794213,290.331818632679,290.415565365381,290.499209042397,
290.582769786463,290.66626764842,290.749730148983,290.833175284475,290.916621119318,
291.000085714556,291.083638899978,291.16723673355,291.250968296412,291.330802134878,
291.413301422989,291.495698257986,291.579750573694,291.662002862286,291.744222964866,
291.826429921203,291.911851636815,291.994123176061,292.076431114752,292.158825062872,
292.168116783652),.UNSPECIFIED.);
#460=B_SPLINE_CURVE_WITH_KNOTS('',3,(#56476,#56477,#56478,#56479,#56480,
#56481,#56482,#56483,#56484,#56485,#56486,#56487,#56488,#56489,#56490,#56491,
#56492,#56493,#56494,#56495,#56496,#56497,#56498,#56499,#56500,#56501,#56502,
#56503,#56504,#56505,#56506,#56507,#56508,#56509,#56510,#56511,#56512,#56513,
#56514,#56515,#56516,#56517,#56518,#56519,#56520,#56521,#56522,#56523,#56524,
#56525,#56526,#56527,#56528,#56529,#56530,#56531,#56532,#56533,#56534,#56535,
#56536,#56537,#56538,#56539,#56540,#56541,#56542,#56543,#56544,#56545,#56546,
#56547,#56548,#56549,#56550,#56551,#56552,#56553,#56554,#56555,#56556,#56557,
#56558,#56559,#56560,#56561,#56562,#56563,#56564,#56565,#56566,#56567,#56568,
#56569,#56570,#56571,#56572,#56573,#56574,#56575,#56576,#56577,#56578,#56579,
#56580,#56581,#56582,#56583,#56584,#56585,#56586,#56587,#56588,#56589,#56590,
#56591,#56592,#56593,#56594,#56595,#56596,#56597,#56598,#56599,#56600,#56601,
#56602,#56603,#56604,#56605,#56606,#56607,#56608,#56609,#56610,#56611,#56612,
#56613,#56614,#56615,#56616,#56617,#56618,#56619,#56620,#56621,#56622,#56623,
#56624,#56625,#56626,#56627,#56628,#56629,#56630,#56631,#56632,#56633,#56634,
#56635,#56636,#56637,#56638,#56639,#56640,#56641,#56642,#56643,#56644,#56645,
#56646,#56647,#56648,#56649,#56650,#56651,#56652,#56653,#56654,#56655,#56656,
#56657,#56658,#56659,#56660,#56661,#56662,#56663,#56664,#56665,#56666,#56667,
#56668,#56669,#56670,#56671,#56672,#56673,#56674,#56675,#56676,#56677,#56678,
#56679,#56680,#56681,#56682,#56683,#56684,#56685,#56686,#56687,#56688,#56689,
#56690,#56691,#56692,#56693,#56694,#56695,#56696,#56697,#56698,#56699,#56700,
#56701),.UNSPECIFIED.,.F.,.F.,(4,3,3,3,3,3,3,3,3,3,3,3,3,3,3,3,3,3,3,3,
3,3,3,3,3,3,3,3,3,3,3,3,3,3,3,3,3,3,3,3,3,3,3,3,3,3,3,3,3,3,3,3,3,3,3,3,
3,3,3,3,3,3,3,3,3,3,3,3,3,3,3,3,3,3,3,4),(292.168116783852,292.30350733608,
292.329785637078,292.41353236978,292.497176046796,292.580736790862,292.664234652819,
292.747697153381,292.831142288874,292.914588123716,292.998052718955,293.081605904376,
293.165203737949,293.248935300811,293.328769139277,293.412515871979,293.496159548995,
293.579720293061,293.663218155018,293.74668065558,293.830125791073,293.913571625915,
293.997036221153,294.080589406575,294.164187240148,294.24791880301,294.327752641476,
294.411499374178,294.495143051194,294.578703795261,294.662201657217,294.74566415778,
294.829109293272,294.912555128115,294.996019723353,295.079572908775,295.163170742348,
295.24690230521,295.326736143675,295.410482876377,295.494126553393,295.577687297459,
295.661185159416,295.744647659978,295.82809279547,295.911538630313,295.995003225551,
296.078556410973,296.162154244545,296.245885807407,296.325719645874,296.409466378576,
296.493110055592,296.576670799659,296.660168661615,296.743631162178,296.82707629767,
296.910522132513,296.993986727751,297.077539913173,297.161137746746,297.244869309608,
297.324703148073,297.408449880775,297.492093557791,297.575654301857,297.659152163814,
297.742614664376,297.826059799869,297.909505634711,297.99297022995,298.076523415372,
298.160121248944,298.243852811806,298.323686650273,298.451302091031),
 .UNSPECIFIED.);
#461=B_SPLINE_CURVE_WITH_KNOTS('',3,(#56703,#56704,#56705,#56706,#56707,
#56708,#56709,#56710,#56711,#56712,#56713,#56714,#56715,#56716,#56717,#56718,
#56719,#56720,#56721,#56722,#56723,#56724,#56725,#56726,#56727,#56728,#56729,
#56730,#56731,#56732,#56733,#56734,#56735,#56736,#56737,#56738,#56739,#56740,
#56741,#56742,#56743,#56744,#56745,#56746,#56747,#56748,#56749,#56750,#56751,
#56752,#56753,#56754,#56755,#56756,#56757,#56758,#56759,#56760,#56761,#56762,
#56763,#56764,#56765,#56766,#56767,#56768,#56769,#56770,#56771,#56772,#56773,
#56774,#56775,#56776,#56777,#56778,#56779,#56780,#56781,#56782,#56783,#56784,
#56785,#56786,#56787,#56788,#56789,#56790,#56791,#56792,#56793,#56794,#56795,
#56796,#56797,#56798,#56799,#56800,#56801,#56802,#56803,#56804,#56805,#56806,
#56807,#56808,#56809,#56810,#56811,#56812,#56813,#56814,#56815,#56816,#56817,
#56818,#56819,#56820,#56821,#56822,#56823,#56824,#56825,#56826,#56827,#56828,
#56829,#56830,#56831,#56832,#56833,#56834,#56835,#56836,#56837,#56838,#56839,
#56840,#56841,#56842,#56843,#56844,#56845,#56846,#56847,#56848,#56849,#56850,
#56851,#56852,#56853,#56854,#56855,#56856,#56857,#56858,#56859,#56860,#56861,
#56862,#56863,#56864,#56865,#56866,#56867,#56868,#56869,#56870,#56871,#56872,
#56873,#56874,#56875,#56876,#56877,#56878,#56879,#56880,#56881,#56882,#56883,
#56884,#56885,#56886,#56887,#56888,#56889,#56890,#56891,#56892,#56893,#56894,
#56895,#56896,#56897,#56898,#56899,#56900,#56901,#56902,#56903,#56904,#56905,
#56906,#56907,#56908,#56909,#56910,#56911,#56912,#56913,#56914,#56915,#56916,
#56917,#56918,#56919,#56920,#56921,#56922,#56923,#56924,#56925,#56926,#56927,
#56928,#56929,#56930,#56931),.UNSPECIFIED.,.F.,.F.,(4,3,3,3,3,3,3,3,3,3,
3,3,3,3,3,3,3,3,3,3,3,3,3,3,3,3,3,3,3,3,3,3,3,3,3,3,3,3,3,3,3,3,3,3,3,3,
3,3,3,3,3,3,3,3,3,3,3,3,3,3,3,3,3,3,3,3,3,3,3,3,3,3,3,3,3,3,4),(298.45130209116,
298.533796201892,298.61620327727,298.698544427693,298.780847073419,298.86313145376,
298.945416555541,299.027721363881,299.110111676385,299.192549242173,299.27510847894,
299.322670152472,299.406416885174,299.49006056219,299.573621306256,299.657119168213,
299.740581668776,299.824026804268,299.907472639111,299.990937234349,300.074490419771,
300.158088253344,300.241819816205,300.321653654671,300.405400387373,300.489044064389,
300.572604808455,300.656102670412,300.739565170975,300.823010306467,300.90645614131,
300.989920736548,301.07347392197,301.157071755543,301.240803318404,301.32063715687,
301.404383889572,301.488027566588,301.571588310654,301.655086172611,301.738548673173,
301.821993808665,301.905439643508,301.988904238746,302.072457424168,302.15605525774,
302.239786820602,302.319620659069,302.403367391771,302.487011068787,302.570571812853,
302.65406967481,302.737532175372,302.820977310864,302.904423145707,302.987887740945,
303.071440926367,303.15503875994,303.238770322802,303.318604161268,303.40235089397,
303.485994570986,303.569555315052,303.653053177009,303.736515677572,303.819960813064,
303.903406647907,303.986871243145,304.070424428567,304.15402226214,304.237753825002,
304.317587663468,304.409695946908,304.501451373444,304.59298093114,304.684152418828,
304.734487398054),.UNSPECIFIED.);
#462=B_SPLINE_CURVE_WITH_KNOTS('',3,(#56933,#56934,#56935,#56936,#56937,
#56938,#56939,#56940,#56941,#56942,#56943,#56944,#56945,#56946,#56947,#56948,
#56949,#56950,#56951,#56952,#56953,#56954,#56955,#56956,#56957,#56958,#56959,
#56960,#56961,#56962,#56963,#56964,#56965,#56966,#56967,#56968,#56969,#56970,
#56971,#56972,#56973,#56974,#56975,#56976,#56977,#56978,#56979,#56980,#56981,
#56982,#56983,#56984,#56985,#56986,#56987,#56988,#56989,#56990,#56991,#56992,
#56993,#56994,#56995,#56996,#56997,#56998,#56999,#57000,#57001,#57002,#57003,
#57004,#57005,#57006,#57007,#57008,#57009,#57010,#57011,#57012,#57013,#57014,
#57015,#57016,#57017,#57018,#57019,#57020,#57021,#57022,#57023,#57024,#57025,
#57026,#57027,#57028,#57029,#57030,#57031,#57032,#57033,#57034,#57035,#57036,
#57037,#57038,#57039,#57040,#57041,#57042,#57043,#57044,#57045,#57046,#57047,
#57048,#57049,#57050,#57051,#57052,#57053,#57054,#57055,#57056,#57057,#57058,
#57059,#57060,#57061,#57062,#57063,#57064,#57065,#57066,#57067,#57068,#57069,
#57070,#57071,#57072,#57073,#57074,#57075,#57076,#57077,#57078,#57079,#57080,
#57081,#57082,#57083,#57084,#57085,#57086,#57087,#57088,#57089,#57090,#57091,
#57092,#57093,#57094,#57095,#57096,#57097,#57098,#57099,#57100,#57101,#57102,
#57103,#57104,#57105,#57106,#57107,#57108,#57109,#57110,#57111,#57112,#57113,
#57114,#57115,#57116,#57117,#57118,#57119,#57120,#57121,#57122,#57123,#57124,
#57125,#57126,#57127,#57128,#57129,#57130,#57131,#57132,#57133,#57134,#57135,
#57136,#57137,#57138,#57139,#57140,#57141,#57142,#57143,#57144,#57145,#57146,
#57147,#57148,#57149,#57150,#57151,#57152,#57153,#57154,#57155,#57156,#57157,
#57158,#57159,#57160,#57161),.UNSPECIFIED.,.F.,.F.,(4,3,3,3,3,3,3,3,3,3,
3,3,3,3,3,3,3,3,3,3,3,3,3,3,3,3,3,3,3,3,3,3,3,3,3,3,3,3,3,3,3,3,3,3,3,3,
3,3,3,3,3,3,3,3,3,3,3,3,3,3,3,3,3,3,3,3,3,3,3,3,3,3,3,3,3,3,4),(304.734487398211,
304.81944881686,304.904444162665,304.989489045624,305.074661256914,305.159900318433,
305.24529683897,305.316571165667,305.400317898369,305.483961575385,305.567522319451,
305.651020181408,305.734482681971,305.817927817463,305.901373652306,305.984838247544,
306.068391432966,306.151989266538,306.2357208294,306.315554667866,306.399301400568,
306.482945077584,306.566505821651,306.650003683608,306.73346618417,306.816911319663,
306.900357154506,306.983821749744,307.067374935166,307.150972768739,307.2347043316,
307.314538170065,307.398284902767,307.481928579782,307.565489323849,307.648987185805,
307.732449686368,307.81589482186,307.899340656703,307.982805251941,308.066358437362,
308.149956270935,308.233687833796,308.313521672264,308.397268404966,308.480912081982,
308.564472826049,308.647970688006,308.731433188568,308.814878324061,308.898324158904,
308.981788754142,309.065341939564,309.148939773137,309.232671335999,309.312505174463,
309.396251907165,309.479895584181,309.563456328248,309.646954190205,309.730416690767,
309.813861826259,309.897307661102,309.98077225634,310.064325441762,310.147923275334,
310.231654838196,310.311488676663,310.394680301707,310.477737958829,310.560718133827,
310.643639475125,310.726520583928,310.809394585425,310.892263754866,310.975171847956,
311.01767270539),.UNSPECIFIED.);
#463=B_SPLINE_CURVE_WITH_KNOTS('',3,(#57163,#57164,#57165,#57166,#57167,
#57168,#57169,#57170,#57171,#57172,#57173,#57174,#57175,#57176,#57177,#57178,
#57179,#57180,#57181,#57182,#57183,#57184,#57185,#57186,#57187,#57188,#57189,
#57190,#57191,#57192,#57193,#57194,#57195,#57196,#57197,#57198,#57199,#57200,
#57201,#57202,#57203,#57204,#57205,#57206,#57207,#57208,#57209,#57210,#57211,
#57212,#57213,#57214,#57215,#57216,#57217,#57218,#57219,#57220,#57221,#57222,
#57223,#57224,#57225,#57226,#57227,#57228,#57229,#57230,#57231,#57232,#57233,
#57234,#57235,#57236,#57237,#57238,#57239,#57240,#57241,#57242,#57243,#57244,
#57245,#57246,#57247,#57248,#57249,#57250,#57251,#57252,#57253,#57254,#57255,
#57256,#57257,#57258,#57259,#57260,#57261,#57262,#57263,#57264,#57265,#57266,
#57267,#57268,#57269,#57270,#57271,#57272,#57273,#57274,#57275,#57276,#57277,
#57278,#57279,#57280,#57281,#57282,#57283,#57284,#57285,#57286,#57287,#57288,
#57289,#57290,#57291,#57292,#57293,#57294,#57295,#57296,#57297,#57298,#57299,
#57300,#57301,#57302,#57303,#57304,#57305,#57306,#57307,#57308,#57309,#57310,
#57311,#57312,#57313,#57314,#57315,#57316,#57317,#57318,#57319,#57320,#57321,
#57322,#57323,#57324,#57325,#57326,#57327,#57328,#57329,#57330,#57331,#57332,
#57333,#57334,#57335,#57336,#57337,#57338,#57339,#57340,#57341,#57342,#57343,
#57344,#57345,#57346,#57347,#57348,#57349,#57350,#57351,#57352,#57353,#57354,
#57355,#57356,#57357,#57358,#57359,#57360,#57361,#57362,#57363,#57364,#57365,
#57366,#57367,#57368,#57369,#57370,#57371,#57372,#57373,#57374,#57375,#57376,
#57377,#57378,#57379,#57380,#57381,#57382,#57383,#57384,#57385,#57386,#57387,
#57388),.UNSPECIFIED.,.F.,.F.,(4,3,3,3,3,3,3,3,3,3,3,3,3,3,3,3,3,3,3,3,
3,3,3,3,3,3,3,3,3,3,3,3,3,3,3,3,3,3,3,3,3,3,3,3,3,3,3,3,3,3,3,3,3,3,3,3,
3,3,3,3,3,3,3,3,3,3,3,3,3,3,3,3,3,3,3,4),(311.017672705525,311.118994588861,
311.221737110735,311.310472178862,311.394218911564,311.47786258858,311.561423332646,
311.644921194603,311.728383695166,311.811828830658,311.895274665501,311.978739260739,
312.06229244616,312.145890279733,312.229621842595,312.309455681061,312.393202413763,
312.476846090779,312.560406834845,312.643904696802,312.727367197364,312.810812332857,
312.894258167699,312.977722762938,313.061275948359,313.144873781932,313.228605344794,
313.30843918326,313.392185915962,313.475829592978,313.559390337044,313.642888199001,
313.726350699563,313.809795835055,313.893241669898,313.976706265136,314.060259450558,
314.143857284131,314.227588846992,314.307422685459,314.391169418161,314.474813095177,
314.558373839243,314.6418717012,314.725334201763,314.808779337255,314.892225172098,
314.975689767336,315.059242952758,315.142840786331,315.226572349193,315.306406187658,
315.39015292036,315.473796597376,315.557357341442,315.640855203399,315.724317703962,
315.807762839454,315.891208674297,315.974673269535,316.058226454957,316.14182428853,
316.225555851391,316.305389689858,316.389083466982,316.472674214911,316.556182113853,
316.639627271712,316.723037303317,316.806430203246,316.889824087096,316.973237067301,
317.056738640507,317.140285262128,317.223964649307,317.300858012433),
 .UNSPECIFIED.);
#464=B_SPLINE_CURVE_WITH_KNOTS('',3,(#57390,#57391,#57392,#57393,#57394,
#57395,#57396,#57397,#57398,#57399,#57400,#57401,#57402,#57403,#57404,#57405,
#57406,#57407,#57408,#57409,#57410,#57411,#57412,#57413,#57414,#57415,#57416,
#57417,#57418,#57419,#57420,#57421,#57422,#57423,#57424,#57425,#57426,#57427,
#57428,#57429,#57430,#57431,#57432,#57433,#57434,#57435,#57436,#57437,#57438,
#57439,#57440,#57441,#57442,#57443,#57444,#57445,#57446,#57447,#57448,#57449,
#57450,#57451,#57452,#57453,#57454,#57455,#57456,#57457,#57458,#57459,#57460,
#57461,#57462,#57463,#57464,#57465,#57466,#57467,#57468,#57469,#57470,#57471,
#57472,#57473,#57474,#57475,#57476,#57477,#57478,#57479,#57480,#57481,#57482,
#57483,#57484,#57485,#57486,#57487,#57488,#57489,#57490,#57491,#57492,#57493,
#57494,#57495,#57496,#57497,#57498,#57499,#57500,#57501,#57502,#57503,#57504,
#57505,#57506,#57507,#57508,#57509,#57510,#57511,#57512,#57513,#57514,#57515,
#57516,#57517,#57518,#57519,#57520,#57521,#57522,#57523,#57524,#57525,#57526,
#57527,#57528,#57529,#57530,#57531,#57532,#57533,#57534,#57535,#57536,#57537,
#57538,#57539,#57540,#57541,#57542,#57543,#57544,#57545,#57546,#57547,#57548,
#57549,#57550,#57551,#57552,#57553,#57554,#57555,#57556,#57557,#57558,#57559,
#57560,#57561,#57562,#57563,#57564,#57565,#57566,#57567,#57568,#57569,#57570,
#57571,#57572,#57573,#57574,#57575,#57576,#57577,#57578,#57579,#57580,#57581,
#57582,#57583,#57584,#57585,#57586,#57587,#57588,#57589,#57590,#57591,#57592,
#57593,#57594,#57595,#57596,#57597,#57598,#57599,#57600,#57601,#57602,#57603,
#57604,#57605,#57606,#57607,#57608,#57609,#57610,#57611,#57612,#57613,#57614,
#57615,#57616,#57617,#57618),.UNSPECIFIED.,.F.,.F.,(4,3,3,3,3,3,3,3,3,3,
3,3,3,3,3,3,3,3,3,3,3,3,3,3,3,3,3,3,3,3,3,3,3,3,3,3,3,3,3,3,3,3,3,3,3,3,
3,3,3,3,3,3,3,3,3,3,3,3,3,3,3,3,3,3,3,3,3,3,3,3,3,3,3,3,3,3,4),(317.30085801257,
317.304373192057,317.388119924759,317.471763601775,317.555324345842,317.638822207799,
317.722284708361,317.805729843854,317.889175678697,317.972640273935,318.056193459357,
318.13979129293,318.223522855791,318.303356694256,318.387103426958,318.470747103974,
318.55430784804,318.637805709997,318.721268210559,318.804713346052,318.888159180894,
318.971623776132,319.055176961554,319.138774795127,319.222506357989,319.302340196455,
319.386086929157,319.469730606173,319.553291350239,319.636789212196,319.720251712759,
319.803696848251,319.887142683094,319.970607278332,320.054160463754,320.137758297326,
320.221489860188,320.301323698654,320.385070431356,320.468714108372,320.552274852438,
320.635772714395,320.719235214958,320.80268035045,320.886126185293,320.969590780531,
321.053143965953,321.136741799525,321.220473362387,321.300307200853,321.384053933555,
321.467697610571,321.551258354637,321.634756216594,321.718218717157,321.801663852649,
321.885109687492,321.96857428273,322.052127468152,322.135725301725,322.219456864587,
322.299290703053,322.383037435755,322.466681112771,322.550241856837,322.633739718794,
322.717202219357,322.800647354849,322.884093189692,322.96755778493,323.051110970352,
323.134708803925,323.218440366787,323.298274205252,323.402181613344,323.504610985504,
323.584043319628),.UNSPECIFIED.);
#465=B_SPLINE_CURVE_WITH_KNOTS('',3,(#57620,#57621,#57622,#57623,#57624,
#57625,#57626,#57627,#57628,#57629,#57630,#57631,#57632,#57633,#57634,#57635,
#57636,#57637,#57638,#57639,#57640,#57641,#57642,#57643,#57644,#57645,#57646,
#57647,#57648,#57649,#57650,#57651,#57652,#57653,#57654,#57655,#57656,#57657,
#57658,#57659,#57660,#57661,#57662,#57663,#57664,#57665,#57666,#57667,#57668,
#57669,#57670,#57671,#57672,#57673,#57674,#57675,#57676,#57677,#57678,#57679,
#57680,#57681,#57682,#57683,#57684,#57685,#57686,#57687,#57688,#57689,#57690,
#57691,#57692,#57693,#57694,#57695,#57696,#57697,#57698,#57699,#57700,#57701,
#57702,#57703,#57704,#57705,#57706,#57707,#57708,#57709,#57710,#57711,#57712,
#57713,#57714,#57715,#57716,#57717,#57718,#57719,#57720,#57721,#57722,#57723,
#57724,#57725,#57726,#57727,#57728,#57729,#57730,#57731,#57732,#57733,#57734,
#57735,#57736,#57737,#57738,#57739,#57740,#57741,#57742,#57743,#57744,#57745,
#57746,#57747,#57748,#57749,#57750,#57751,#57752,#57753,#57754,#57755,#57756,
#57757,#57758,#57759,#57760,#57761,#57762,#57763,#57764,#57765,#57766,#57767,
#57768,#57769,#57770,#57771,#57772,#57773,#57774,#57775,#57776,#57777,#57778,
#57779,#57780,#57781,#57782,#57783,#57784,#57785,#57786,#57787,#57788,#57789,
#57790,#57791,#57792,#57793,#57794,#57795,#57796,#57797,#57798,#57799,#57800,
#57801,#57802,#57803,#57804,#57805,#57806,#57807,#57808,#57809,#57810,#57811,
#57812,#57813,#57814,#57815,#57816,#57817,#57818,#57819,#57820,#57821,#57822,
#57823,#57824,#57825,#57826,#57827,#57828,#57829,#57830,#57831,#57832,#57833,
#57834,#57835,#57836,#57837,#57838,#57839,#57840,#57841,#57842,#57843,#57844,
#57845,#57846,#57847,#57848),.UNSPECIFIED.,.F.,.F.,(4,3,3,3,3,3,3,3,3,3,
3,3,3,3,3,3,3,3,3,3,3,3,3,3,3,3,3,3,3,3,3,3,3,3,3,3,3,3,3,3,3,3,3,3,3,3,
3,3,3,3,3,3,3,3,3,3,3,3,3,3,3,3,3,3,3,3,3,3,3,3,3,3,3,3,3,3,4),(323.58404331975,
323.666886187998,323.749698014738,323.83249604088,323.915298875906,323.998125129485,
324.081041926353,324.164008541604,324.247101083384,324.297257707451,324.381004440153,
324.464648117169,324.548208861235,324.631706723192,324.715169223755,324.798614359247,
324.88206019409,324.965524789328,325.04907797475,325.132675808322,325.216407371184,
325.29624120965,325.379987942352,325.463631619368,325.547192363434,325.630690225391,
325.714152725954,325.797597861446,325.881043696289,325.964508291527,326.048061476949,
326.131659310521,326.215390873383,326.295224711849,326.378971444551,326.462615121567,
326.546175865634,326.629673727591,326.713136228153,326.796581363646,326.880027198489,
326.963491793727,327.047044979149,327.130642812722,327.214374375583,327.294208214048,
327.37795494675,327.461598623766,327.545159367832,327.628657229789,327.712119730352,
327.795564865844,327.879010700687,327.962475295925,328.046028481347,328.129626314919,
328.213357877781,328.293191716248,328.37693844895,328.460582125966,328.544142870033,
328.627640731989,328.711103232552,328.794548368044,328.877994202887,328.961458798126,
329.045011983548,329.12860981712,329.212341379982,329.292175218447,329.377761784272,
329.463229543,329.548594014623,329.633848460025,329.71903832337,329.804171773391,
329.867228626929),.UNSPECIFIED.);
#466=B_SPLINE_CURVE_WITH_KNOTS('',3,(#57850,#57851,#57852,#57853,#57854,
#57855,#57856,#57857,#57858,#57859,#57860,#57861,#57862,#57863,#57864,#57865,
#57866,#57867,#57868,#57869,#57870,#57871,#57872,#57873,#57874,#57875,#57876,
#57877,#57878,#57879,#57880,#57881,#57882,#57883,#57884,#57885,#57886,#57887,
#57888,#57889,#57890,#57891,#57892,#57893,#57894,#57895,#57896,#57897,#57898,
#57899,#57900,#57901,#57902,#57903,#57904,#57905,#57906,#57907,#57908,#57909,
#57910,#57911,#57912,#57913,#57914,#57915,#57916,#57917,#57918,#57919,#57920,
#57921,#57922,#57923,#57924,#57925,#57926,#57927,#57928,#57929,#57930,#57931,
#57932,#57933,#57934,#57935,#57936,#57937,#57938,#57939,#57940,#57941,#57942,
#57943,#57944,#57945,#57946,#57947,#57948,#57949,#57950,#57951,#57952,#57953,
#57954,#57955,#57956,#57957,#57958,#57959,#57960,#57961,#57962,#57963,#57964,
#57965,#57966,#57967,#57968,#57969,#57970,#57971,#57972,#57973,#57974,#57975,
#57976,#57977,#57978,#57979,#57980,#57981,#57982,#57983,#57984,#57985,#57986,
#57987,#57988,#57989,#57990,#57991,#57992,#57993,#57994,#57995,#57996,#57997,
#57998,#57999,#58000,#58001,#58002,#58003,#58004,#58005,#58006,#58007,#58008,
#58009,#58010,#58011,#58012,#58013,#58014,#58015,#58016,#58017,#58018,#58019,
#58020,#58021,#58022,#58023,#58024,#58025,#58026,#58027,#58028,#58029,#58030,
#58031,#58032,#58033,#58034,#58035,#58036,#58037,#58038,#58039,#58040,#58041,
#58042,#58043,#58044,#58045,#58046,#58047,#58048,#58049,#58050,#58051,#58052,
#58053,#58054,#58055,#58056,#58057,#58058,#58059,#58060,#58061,#58062,#58063,
#58064,#58065,#58066,#58067,#58068,#58069,#58070,#58071,#58072,#58073,#58074,
#58075,#58076,#58077,#58078),.UNSPECIFIED.,.F.,.F.,(4,3,3,3,3,3,3,3,3,3,
3,3,3,3,3,3,3,3,3,3,3,3,3,3,3,3,3,3,3,3,3,3,3,3,3,3,3,3,3,3,3,3,3,3,3,3,
3,3,3,3,3,3,3,3,3,3,3,3,3,3,3,3,3,3,3,3,3,3,3,3,3,3,3,3,3,3,4),(329.86722862708,
329.957952637098,330.049077582971,330.140406534098,330.232041447377,330.291158720646,
330.374905453348,330.458549130364,330.542109874431,330.625607736387,330.70907023695,
330.792515372442,330.875961207285,330.959425802523,331.042978987945,331.126576821518,
331.21030838438,331.290142222845,331.373888955547,331.457532632563,331.541093376629,
331.624591238586,331.708053739148,331.79149887464,331.874944709483,331.958409304721,
332.041962490143,332.125560323716,332.209291886577,332.289125725044,332.372872457746,
332.456516134762,332.540076878828,332.623574740785,332.707037241348,332.79048237684,
332.873928211683,332.957392806921,333.040945992343,333.124543825916,333.208275388778,
333.288109227243,333.371855959945,333.455499636961,333.539060381027,333.622558242984,
333.706020743547,333.789465879039,333.872911713882,333.95637630912,334.039929494541,
334.123527328114,334.207258890976,334.287092729443,334.370839462145,334.454483139161,
334.538043883227,334.621541745184,334.705004245747,334.788449381239,334.871895216082,
334.95535981132,335.038912996742,335.122510830315,335.206242393176,335.286076231642,
335.368622249699,335.451066024559,335.533428752273,335.615730097583,335.697999133896,
335.780254872469,335.862516310863,335.944840664036,336.027200299695,336.109659708555,
336.150413933984),.UNSPECIFIED.);
#467=B_SPLINE_CURVE_WITH_KNOTS('',3,(#58080,#58081,#58082,#58083,#58084,
#58085,#58086,#58087,#58088,#58089,#58090,#58091,#58092,#58093,#58094,#58095,
#58096,#58097,#58098,#58099,#58100,#58101,#58102,#58103,#58104,#58105,#58106,
#58107,#58108,#58109,#58110,#58111,#58112,#58113,#58114,#58115,#58116,#58117,
#58118,#58119,#58120,#58121,#58122,#58123,#58124,#58125,#58126,#58127,#58128,
#58129,#58130,#58131,#58132,#58133,#58134,#58135,#58136,#58137,#58138,#58139,
#58140,#58141,#58142,#58143,#58144,#58145,#58146,#58147,#58148,#58149,#58150,
#58151,#58152,#58153,#58154,#58155,#58156,#58157,#58158,#58159,#58160,#58161,
#58162,#58163,#58164,#58165,#58166,#58167,#58168,#58169,#58170,#58171,#58172,
#58173,#58174,#58175,#58176,#58177,#58178,#58179,#58180,#58181,#58182,#58183,
#58184,#58185,#58186,#58187,#58188,#58189,#58190,#58191,#58192,#58193,#58194,
#58195,#58196,#58197,#58198,#58199,#58200,#58201,#58202,#58203,#58204,#58205,
#58206,#58207,#58208,#58209,#58210,#58211,#58212,#58213,#58214,#58215,#58216,
#58217,#58218,#58219,#58220,#58221,#58222,#58223,#58224,#58225,#58226,#58227,
#58228,#58229,#58230,#58231,#58232,#58233,#58234,#58235,#58236,#58237,#58238,
#58239,#58240,#58241,#58242,#58243,#58244,#58245,#58246,#58247,#58248,#58249,
#58250,#58251,#58252,#58253,#58254,#58255,#58256,#58257,#58258,#58259,#58260,
#58261,#58262,#58263,#58264,#58265,#58266,#58267,#58268,#58269,#58270,#58271,
#58272,#58273,#58274,#58275,#58276,#58277,#58278,#58279,#58280,#58281,#58282,
#58283,#58284,#58285,#58286,#58287,#58288,#58289,#58290,#58291,#58292,#58293,
#58294,#58295,#58296,#58297,#58298,#58299,#58300,#58301,#58302,#58303,#58304,
#58305),.UNSPECIFIED.,.F.,.F.,(4,3,3,3,3,3,3,3,3,3,3,3,3,3,3,3,3,3,3,3,
3,3,3,3,3,3,3,3,3,3,3,3,3,3,3,3,3,3,3,3,3,3,3,3,3,3,3,3,3,3,3,3,3,3,3,3,
3,3,3,3,3,3,3,3,3,3,3,3,3,3,3,3,3,3,3,4),(336.150413934109,336.285059733841,
336.368806466543,336.452450143559,336.536010887625,336.619508749582,336.702971250145,
336.786416385637,336.86986222048,336.953326815718,337.03688000114,337.120477834713,
337.204209397575,337.28404323604,337.367789968742,337.451433645758,337.534994389824,
337.618492251781,337.701954752344,337.785399887836,337.868845722679,337.952310317917,
338.035863503339,338.119461336911,338.203192899773,338.283026738239,338.366773470941,
338.450417147957,338.533977892023,338.61747575398,338.700938254542,338.784383390035,
338.867829224877,338.951293820115,339.034847005537,339.11844483911,339.202176401972,
339.282010240438,339.36575697314,339.449400650156,339.532961394223,339.61645925618,
339.699921756742,339.783366892235,339.866812727078,339.950277322316,340.033830507738,
340.117428341311,340.201159904173,340.280993742638,340.36474047534,340.448384152356,
340.531944896422,340.615442758379,340.698905258942,340.782350394434,340.865796229277,
340.949260824515,341.032814009937,341.11641184351,341.200143406372,341.279977244837,
341.363723977539,341.447367654555,341.530928398621,341.614426260578,341.69788876114,
341.781333896633,341.864779731475,341.948244326713,342.031797512135,342.115395345708,
342.199126908569,342.278960747036,342.418201063665,342.433599241288),
 .UNSPECIFIED.);
#468=B_SPLINE_CURVE_WITH_KNOTS('',3,(#58307,#58308,#58309,#58310,#58311,
#58312,#58313,#58314,#58315,#58316,#58317,#58318,#58319,#58320,#58321,#58322,
#58323,#58324,#58325,#58326,#58327,#58328,#58329,#58330,#58331,#58332,#58333,
#58334,#58335,#58336,#58337,#58338,#58339,#58340,#58341,#58342,#58343,#58344,
#58345,#58346,#58347,#58348,#58349,#58350,#58351,#58352,#58353,#58354,#58355,
#58356,#58357,#58358,#58359,#58360,#58361,#58362,#58363,#58364,#58365,#58366,
#58367,#58368,#58369,#58370,#58371,#58372,#58373,#58374,#58375,#58376,#58377,
#58378,#58379,#58380,#58381,#58382,#58383,#58384,#58385,#58386,#58387,#58388,
#58389,#58390,#58391,#58392,#58393,#58394,#58395,#58396,#58397,#58398,#58399,
#58400,#58401,#58402,#58403,#58404,#58405,#58406,#58407,#58408,#58409,#58410,
#58411,#58412,#58413,#58414,#58415,#58416,#58417,#58418,#58419,#58420,#58421,
#58422,#58423,#58424,#58425,#58426,#58427,#58428,#58429,#58430,#58431,#58432,
#58433,#58434,#58435,#58436,#58437,#58438,#58439,#58440,#58441,#58442,#58443,
#58444,#58445,#58446,#58447,#58448,#58449,#58450,#58451,#58452,#58453,#58454,
#58455,#58456,#58457,#58458,#58459,#58460,#58461,#58462,#58463,#58464,#58465,
#58466,#58467,#58468,#58469,#58470,#58471,#58472,#58473,#58474,#58475,#58476,
#58477,#58478,#58479,#58480,#58481,#58482,#58483,#58484,#58485,#58486,#58487,
#58488,#58489,#58490,#58491,#58492,#58493,#58494,#58495,#58496,#58497,#58498,
#58499,#58500,#58501,#58502,#58503,#58504,#58505,#58506,#58507,#58508,#58509,
#58510,#58511,#58512,#58513,#58514,#58515,#58516,#58517,#58518,#58519,#58520,
#58521,#58522,#58523,#58524,#58525,#58526,#58527,#58528,#58529,#58530,#58531,
#58532,#58533,#58534,#58535),.UNSPECIFIED.,.F.,.F.,(4,3,3,3,3,3,3,3,3,3,
3,3,3,3,3,3,3,3,3,3,3,3,3,3,3,3,3,3,3,3,3,3,3,3,3,3,3,3,3,3,3,3,3,3,3,3,
3,3,3,3,3,3,3,3,3,3,3,3,3,3,3,3,3,3,3,3,3,3,3,3,3,3,3,3,3,3,4),(342.433599241396,
342.516002347129,342.598324574841,342.68327703414,342.765508333302,342.847727632491,
342.929953955044,343.01220632799,343.094547026574,343.1769407611,343.259448331164,
343.277944249235,343.361690981937,343.445334658953,343.528895403019,343.612393264976,
343.695855765538,343.77930090103,343.862746735873,343.946211331111,344.029764516533,
344.113362350106,344.197093912967,344.276927751434,344.360674484136,344.444318161152,
344.527878905218,344.611376767175,344.694839267738,344.77828440323,344.861730238073,
344.94519483331,345.028748018732,345.112345852305,345.196077415167,345.275911253633,
345.359657986335,345.443301663351,345.526862407418,345.610360269374,345.693822769937,
345.777267905429,345.860713740272,345.94417833551,346.027731520932,346.111329354504,
346.195060917366,346.274894755833,346.358641488535,346.442285165551,346.525845909618,
346.609343771575,346.692806272137,346.77625140763,346.859697242473,346.943161837711,
347.026715023132,347.110312856705,347.194044419567,347.273878258032,347.357624990734,
347.44126866775,347.524829411816,347.608327273773,347.691789774335,347.775234909828,
347.85868074467,347.942145339908,348.02569852533,348.109296358902,348.193027921764,
348.272861760231,348.363449546096,348.453737517769,348.543843582329,348.633659106349,
348.716784548354),.UNSPECIFIED.);
#469=B_SPLINE_CURVE_WITH_KNOTS('',3,(#58537,#58538,#58539,#58540,#58541,
#58542,#58543,#58544,#58545,#58546,#58547,#58548,#58549,#58550,#58551,#58552,
#58553,#58554,#58555,#58556,#58557,#58558,#58559,#58560,#58561,#58562,#58563,
#58564,#58565,#58566,#58567,#58568,#58569,#58570,#58571,#58572,#58573,#58574,
#58575,#58576,#58577,#58578,#58579,#58580,#58581,#58582,#58583,#58584,#58585,
#58586,#58587,#58588,#58589,#58590,#58591,#58592,#58593,#58594,#58595,#58596,
#58597,#58598,#58599,#58600,#58601,#58602,#58603,#58604,#58605,#58606,#58607,
#58608,#58609,#58610,#58611,#58612,#58613,#58614,#58615,#58616,#58617,#58618,
#58619,#58620,#58621,#58622,#58623,#58624,#58625,#58626,#58627,#58628,#58629,
#58630,#58631,#58632,#58633,#58634,#58635,#58636,#58637,#58638,#58639,#58640,
#58641,#58642,#58643,#58644,#58645,#58646,#58647,#58648,#58649,#58650,#58651,
#58652,#58653,#58654,#58655,#58656,#58657,#58658,#58659,#58660,#58661,#58662,
#58663,#58664,#58665,#58666,#58667,#58668,#58669,#58670,#58671,#58672,#58673,
#58674,#58675,#58676,#58677,#58678,#58679,#58680,#58681,#58682,#58683,#58684,
#58685,#58686,#58687,#58688,#58689,#58690,#58691,#58692,#58693,#58694,#58695,
#58696,#58697,#58698,#58699,#58700,#58701,#58702,#58703,#58704,#58705,#58706,
#58707,#58708,#58709,#58710,#58711,#58712,#58713,#58714,#58715,#58716,#58717,
#58718,#58719,#58720,#58721,#58722,#58723,#58724,#58725,#58726,#58727,#58728,
#58729,#58730,#58731,#58732,#58733,#58734,#58735,#58736,#58737,#58738,#58739,
#58740,#58741,#58742,#58743,#58744,#58745,#58746,#58747,#58748,#58749,#58750,
#58751,#58752,#58753,#58754,#58755,#58756,#58757,#58758,#58759,#58760,#58761,
#58762,#58763,#58764,#58765),.UNSPECIFIED.,.F.,.F.,(4,3,3,3,3,3,3,3,3,3,
3,3,3,3,3,3,3,3,3,3,3,3,3,3,3,3,3,3,3,3,3,3,3,3,3,3,3,3,3,3,3,3,3,3,3,3,
3,3,3,3,3,3,3,3,3,3,3,3,3,3,3,3,3,3,3,3,3,3,3,3,3,3,3,3,3,3,4),(348.716784548468,
348.802434990704,348.888140583416,348.973915359868,349.059835222646,349.145836218956,
349.231993934527,349.27184526243,349.355591995132,349.439235672148,349.522796416214,
349.606294278171,349.689756778733,349.773201914226,349.856647749068,349.940112344306,
350.023665529728,350.107263363301,350.190994926162,350.270828764629,350.354575497331,
350.438219174347,350.521779918413,350.60527778037,350.688740280933,350.772185416425,
350.855631251267,350.939095846506,351.022649031927,351.1062468655,351.189978428362,
351.269812266828,351.35355899953,351.437202676546,351.520763420612,351.604261282569,
351.687723783132,351.771168918624,351.854614753467,351.938079348705,352.021632534127,
352.105230367699,352.188961930561,352.268795769027,352.352542501729,352.436186178745,
352.519746922811,352.603244784768,352.686707285331,352.770152420823,352.853598255666,
352.937062850904,353.020616036326,353.104213869899,353.187945432761,353.267779271227,
353.351526003929,353.435169680945,353.518730425011,353.602228286967,353.68569078753,
353.769135923022,353.852581757865,353.936046353103,354.019599538525,354.103197372098,
354.18692893496,354.266762773426,354.349682329874,354.432471146391,354.515184784845,
354.597842098166,354.680461891829,354.763083217737,354.845702109952,354.928375725224,
354.999969855647),.UNSPECIFIED.);
#470=B_SPLINE_CURVE_WITH_KNOTS('',3,(#58767,#58768,#58769,#58770,#58771,
#58772,#58773,#58774,#58775,#58776,#58777,#58778,#58779,#58780,#58781,#58782,
#58783,#58784,#58785,#58786,#58787,#58788,#58789,#58790,#58791,#58792,#58793,
#58794,#58795,#58796,#58797,#58798,#58799,#58800,#58801,#58802,#58803,#58804,
#58805,#58806,#58807,#58808,#58809,#58810,#58811,#58812,#58813,#58814,#58815,
#58816,#58817,#58818,#58819,#58820,#58821,#58822,#58823,#58824,#58825,#58826,
#58827,#58828,#58829,#58830,#58831,#58832,#58833,#58834,#58835,#58836,#58837,
#58838,#58839,#58840,#58841,#58842,#58843,#58844,#58845,#58846,#58847,#58848,
#58849,#58850,#58851,#58852,#58853,#58854,#58855,#58856,#58857,#58858,#58859,
#58860,#58861,#58862,#58863,#58864,#58865,#58866,#58867,#58868,#58869,#58870,
#58871,#58872,#58873,#58874,#58875,#58876,#58877,#58878,#58879,#58880,#58881,
#58882,#58883,#58884,#58885,#58886,#58887,#58888,#58889,#58890,#58891,#58892,
#58893,#58894,#58895,#58896,#58897,#58898,#58899,#58900,#58901,#58902,#58903,
#58904,#58905,#58906,#58907,#58908,#58909,#58910,#58911,#58912,#58913,#58914,
#58915,#58916,#58917,#58918,#58919,#58920,#58921,#58922,#58923,#58924,#58925,
#58926,#58927,#58928,#58929,#58930,#58931,#58932,#58933,#58934,#58935,#58936,
#58937,#58938,#58939,#58940,#58941,#58942,#58943,#58944,#58945,#58946,#58947,
#58948,#58949,#58950,#58951,#58952,#58953,#58954,#58955,#58956,#58957,#58958,
#58959,#58960,#58961,#58962,#58963,#58964,#58965,#58966,#58967,#58968,#58969,
#58970,#58971,#58972,#58973,#58974,#58975,#58976,#58977,#58978,#58979,#58980,
#58981,#58982,#58983,#58984,#58985,#58986,#58987,#58988,#58989,#58990,#58991,
#58992,#58993,#58994,#58995),.UNSPECIFIED.,.F.,.F.,(4,3,3,3,3,3,3,3,3,3,
3,3,3,3,3,3,3,3,3,3,3,3,3,3,3,3,3,3,3,3,3,3,3,3,3,3,3,3,3,3,3,3,3,3,3,3,
3,3,3,3,3,3,3,3,3,3,3,3,3,3,3,3,3,3,3,3,3,3,3,3,3,3,3,3,3,3,4),(354.999969855808,
355.104758748587,355.211493803573,355.265746275625,355.349493008327,355.433136685343,
355.516697429409,355.600195291366,355.683657791929,355.767102927421,355.850548762264,
355.934013357502,356.017566542924,356.101164376497,356.184895939358,356.264729777824,
356.348476510526,356.432120187542,356.515680931608,356.599178793565,356.682641294128,
356.76608642962,356.849532264463,356.932996859701,357.016550045122,357.100147878695,
357.183879441557,357.263713280023,357.347460012725,357.431103689741,357.514664433807,
357.598162295764,357.681624796327,357.765069931819,357.848515766662,357.9319803619,
358.015533547322,358.099131380894,358.182862943756,358.262696782222,358.346443514924,
358.43008719194,358.513647936007,358.597145797963,358.680608298526,358.764053434018,
358.847499268861,358.930963864099,359.014517049521,359.098114883094,359.181846445956,
359.261680284422,359.345427017124,359.42907069414,359.512631438206,359.596129300163,
359.679591800726,359.763036936218,359.846482771061,359.929947366299,360.013500551721,
360.097098385293,360.180829948155,360.260663786621,360.344410519323,360.428054196339,
360.511614940406,360.595112802363,360.678575302925,360.762020438418,360.845466273261,
360.928930868499,361.012484053921,361.096081887494,361.179813450356,361.25964728882,
361.283155162827),.UNSPECIFIED.);
#471=B_SPLINE_CURVE_WITH_KNOTS('',3,(#58997,#58998,#58999,#59000,#59001,
#59002,#59003,#59004,#59005,#59006),.UNSPECIFIED.,.F.,.F.,(4,1,1,1,1,1,
1,4),(361.283158485953,362.258630791019,363.257614293218,364.256597795417,
365.255581297617,366.254564799816,367.253548302015,367.566334031703),
 .UNSPECIFIED.);
#472=B_SPLINE_CURVE_WITH_KNOTS('',3,(#59008,#59009,#59010,#59011,#59012,
#59013,#59014,#59015,#59016,#59017,#59018,#59019,#59020,#59021,#59022,#59023,
#59024,#59025,#59026,#59027,#59028,#59029,#59030,#59031,#59032,#59033,#59034,
#59035,#59036,#59037,#59038,#59039,#59040,#59041,#59042,#59043,#59044,#59045,
#59046,#59047,#59048,#59049,#59050,#59051,#59052,#59053,#59054,#59055,#59056,
#59057,#59058,#59059,#59060,#59061,#59062,#59063,#59064,#59065,#59066,#59067,
#59068,#59069,#59070,#59071,#59072,#59073,#59074,#59075,#59076,#59077,#59078,
#59079,#59080,#59081,#59082,#59083,#59084,#59085,#59086,#59087,#59088,#59089,
#59090,#59091,#59092,#59093,#59094,#59095,#59096,#59097,#59098,#59099,#59100,
#59101,#59102,#59103,#59104,#59105,#59106,#59107,#59108,#59109,#59110,#59111,
#59112,#59113,#59114,#59115,#59116,#59117,#59118,#59119,#59120,#59121,#59122,
#59123,#59124,#59125,#59126,#59127,#59128,#59129,#59130,#59131,#59132,#59133,
#59134,#59135,#59136,#59137,#59138,#59139,#59140,#59141,#59142,#59143,#59144,
#59145,#59146,#59147,#59148,#59149,#59150,#59151,#59152,#59153,#59154,#59155,
#59156,#59157,#59158,#59159,#59160,#59161,#59162,#59163,#59164,#59165,#59166,
#59167,#59168,#59169,#59170,#59171,#59172,#59173,#59174,#59175,#59176,#59177,
#59178,#59179,#59180,#59181,#59182,#59183,#59184,#59185,#59186,#59187,#59188,
#59189,#59190,#59191,#59192,#59193,#59194,#59195,#59196,#59197,#59198,#59199,
#59200,#59201,#59202,#59203,#59204,#59205,#59206,#59207,#59208,#59209,#59210,
#59211,#59212,#59213,#59214,#59215,#59216,#59217,#59218,#59219,#59220,#59221,
#59222,#59223,#59224,#59225,#59226,#59227,#59228,#59229,#59230,#59231,#59232,
#59233,#59234,#59235,#59236),.UNSPECIFIED.,.F.,.F.,(4,3,3,3,3,3,3,3,3,3,
3,3,3,3,3,3,3,3,3,3,3,3,3,3,3,3,3,3,3,3,3,3,3,3,3,3,3,3,3,3,3,3,3,3,3,3,
3,3,3,3,3,3,3,3,3,3,3,3,3,3,3,3,3,3,3,3,3,3,3,3,3,3,3,3,3,3,4),(367.566340470006,
367.652114386782,367.735224242723,367.818330991452,367.90145296639,367.984608507648,
368.06786137521,368.151172612959,368.234603355717,368.252531804214,368.336278536916,
368.419922213932,368.503482957998,368.586980819955,368.670443320517,368.75388845601,
368.837334290852,368.92079888609,369.004352071512,369.087949905085,369.171681467946,
369.251515306413,369.335262039115,369.418905716131,369.502466460197,369.585964322154,
369.669426822717,369.752871958209,369.836317793052,369.91978238829,370.003335573712,
370.086933407285,370.170664970146,370.250498808612,370.334245541314,370.41788921833,
370.501449962396,370.584947824353,370.668410324916,370.751855460408,370.835301295251,
370.918765890489,371.002319075911,371.085916909484,371.169648472346,371.249482310812,
371.333229043514,371.41687272053,371.500433464596,371.583931326553,371.667393827116,
371.750838962608,371.834284797451,371.917749392689,372.001302578111,372.084900411684,
372.168631974546,372.248465813011,372.332212545713,372.415856222729,372.499416966795,
372.582914828751,372.666377329314,372.749822464806,372.833268299649,372.916732894887,
373.000286080309,373.083883913881,373.167615476743,373.24744931521,373.33236473397,
373.41716843778,373.50187711303,373.588789279069,373.673347477172,373.761436627179,
373.849525777186),.UNSPECIFIED.);
#473=B_SPLINE_CURVE_WITH_KNOTS('',3,(#59238,#59239,#59240,#59241,#59242,
#59243,#59244,#59245,#59246,#59247,#59248,#59249,#59250,#59251,#59252,#59253,
#59254,#59255,#59256,#59257,#59258,#59259,#59260,#59261,#59262,#59263,#59264,
#59265,#59266,#59267,#59268,#59269,#59270,#59271,#59272,#59273,#59274,#59275,
#59276,#59277,#59278,#59279,#59280,#59281,#59282,#59283,#59284,#59285,#59286,
#59287,#59288,#59289,#59290,#59291,#59292,#59293,#59294,#59295,#59296,#59297,
#59298,#59299,#59300,#59301,#59302,#59303,#59304,#59305,#59306,#59307,#59308,
#59309,#59310,#59311,#59312,#59313,#59314,#59315,#59316,#59317,#59318,#59319,
#59320,#59321,#59322,#59323,#59324,#59325,#59326,#59327,#59328,#59329,#59330,
#59331,#59332,#59333,#59334,#59335,#59336,#59337,#59338,#59339,#59340,#59341,
#59342,#59343,#59344,#59345,#59346,#59347,#59348,#59349,#59350,#59351,#59352,
#59353,#59354,#59355,#59356,#59357,#59358,#59359,#59360,#59361,#59362,#59363,
#59364,#59365,#59366,#59367,#59368,#59369,#59370,#59371,#59372,#59373,#59374,
#59375,#59376,#59377,#59378,#59379,#59380,#59381,#59382,#59383,#59384,#59385,
#59386,#59387,#59388,#59389,#59390,#59391,#59392,#59393,#59394,#59395,#59396,
#59397,#59398,#59399,#59400,#59401,#59402,#59403,#59404,#59405,#59406,#59407,
#59408,#59409,#59410,#59411,#59412,#59413,#59414,#59415,#59416,#59417,#59418,
#59419,#59420,#59421,#59422,#59423,#59424,#59425,#59426,#59427,#59428,#59429,
#59430,#59431,#59432,#59433,#59434,#59435,#59436,#59437,#59438,#59439,#59440,
#59441,#59442,#59443,#59444,#59445,#59446,#59447,#59448,#59449,#59450,#59451,
#59452,#59453,#59454,#59455,#59456,#59457,#59458,#59459,#59460,#59461,#59462,
#59463,#59464,#59465,#59466),.UNSPECIFIED.,.F.,.F.,(4,3,3,3,3,3,3,3,3,3,
3,3,3,3,3,3,3,3,3,3,3,3,3,3,3,3,3,3,3,3,3,3,3,3,3,3,3,3,3,3,3,3,3,3,3,3,
3,3,3,3,3,3,3,3,3,3,3,3,3,3,3,3,3,3,3,3,3,3,3,3,3,3,3,3,3,3,4),(373.849525777369,
373.94177576414,374.034531391264,374.127549014038,374.220904227471,374.246432817409,
374.330179550111,374.413823227127,374.497383971193,374.58088183315,374.664344333713,
374.747789469205,374.831235304048,374.914699899286,374.998253084708,375.081850918281,
375.165582481142,375.245416319608,375.32916305231,375.412806729326,375.496367473393,
375.579865335349,375.663327835912,375.746772971404,375.830218806247,375.913683401485,
375.997236586907,376.08083442048,376.164565983342,376.244399821807,376.328146554509,
376.411790231525,376.495350975591,376.578848837548,376.66231133811,376.745756473603,
376.829202308445,376.912666903683,376.996220089105,377.079817922678,377.16354948554,
377.243383324007,377.327130056709,377.410773733725,377.494334477792,377.577832339749,
377.661294840311,377.744739975804,377.828185810647,377.911650405885,377.995203591307,
378.078801424879,378.162532987741,378.242366826206,378.326113558908,378.409757235924,
378.49331797999,378.576815841947,378.660278342509,378.743723478002,378.827169312844,
378.910633908082,378.994187093504,379.077784927077,379.161516489938,379.241350328405,
379.324006495365,379.40656044139,379.489033280296,379.571445359309,379.653825094266,
379.736191427966,379.818563289775,379.901003070109,379.983477649875,380.066065261914,
380.132711084231),.UNSPECIFIED.);
#474=B_SPLINE_CURVE_WITH_KNOTS('',3,(#59468,#59469,#59470,#59471,#59472,
#59473,#59474,#59475,#59476,#59477,#59478,#59479,#59480,#59481,#59482,#59483,
#59484,#59485,#59486,#59487,#59488,#59489,#59490,#59491,#59492,#59493,#59494,
#59495,#59496,#59497,#59498,#59499,#59500,#59501,#59502,#59503,#59504,#59505,
#59506,#59507,#59508,#59509,#59510,#59511,#59512,#59513,#59514,#59515,#59516,
#59517,#59518,#59519,#59520,#59521,#59522,#59523,#59524,#59525,#59526,#59527,
#59528,#59529,#59530,#59531,#59532,#59533,#59534,#59535,#59536,#59537,#59538,
#59539,#59540,#59541,#59542,#59543,#59544,#59545,#59546,#59547,#59548,#59549,
#59550,#59551,#59552,#59553,#59554,#59555,#59556,#59557,#59558,#59559,#59560,
#59561,#59562,#59563,#59564,#59565,#59566,#59567,#59568,#59569,#59570,#59571,
#59572,#59573,#59574,#59575,#59576,#59577,#59578,#59579,#59580,#59581,#59582,
#59583,#59584,#59585,#59586,#59587,#59588,#59589,#59590,#59591,#59592,#59593,
#59594,#59595,#59596,#59597,#59598,#59599,#59600,#59601,#59602,#59603,#59604,
#59605,#59606,#59607,#59608,#59609,#59610,#59611,#59612,#59613,#59614,#59615,
#59616,#59617,#59618,#59619,#59620,#59621,#59622,#59623,#59624,#59625,#59626,
#59627,#59628,#59629,#59630,#59631,#59632,#59633,#59634,#59635,#59636,#59637,
#59638,#59639,#59640,#59641,#59642,#59643,#59644,#59645,#59646,#59647,#59648,
#59649,#59650,#59651,#59652,#59653,#59654,#59655,#59656,#59657,#59658,#59659,
#59660,#59661,#59662,#59663,#59664,#59665,#59666,#59667,#59668,#59669,#59670,
#59671,#59672,#59673,#59674,#59675,#59676,#59677,#59678,#59679,#59680,#59681,
#59682,#59683,#59684,#59685,#59686,#59687,#59688,#59689,#59690,#59691,#59692,
#59693),.UNSPECIFIED.,.F.,.F.,(4,3,3,3,3,3,3,3,3,3,3,3,3,3,3,3,3,3,3,3,
3,3,3,3,3,3,3,3,3,3,3,3,3,3,3,3,3,3,3,3,3,3,3,3,3,3,3,3,3,3,3,3,3,3,3,3,
3,3,3,3,3,3,3,3,3,3,3,3,3,3,3,3,3,3,3,4),(380.132711084366,380.240333830604,
380.324080563306,380.407724240322,380.491284984388,380.574782846345,380.658245346908,
380.7416904824,380.825136317243,380.908600912481,380.992154097903,381.075751931475,
381.159483494337,381.239317332803,381.323064065505,381.406707742521,381.490268486588,
381.573766348544,381.657228849107,381.740673984599,381.824119819442,381.90758441468,
381.991137600102,382.074735433675,382.158466996537,382.238300835002,382.322047567704,
382.40569124472,382.489251988787,382.572749850743,382.656212351306,382.739657486798,
382.823103321641,382.90656791688,382.990121102302,383.073718935874,383.157450498736,
383.237284337202,383.321031069904,383.40467474692,383.488235490986,383.571733352943,
383.655195853506,383.738640988998,383.822086823841,383.905551419079,383.9891046045,
384.072702438073,384.156434000935,384.236267839401,384.320014572103,384.403658249119,
384.487218993185,384.570716855142,384.654179355705,384.737624491197,384.82107032604,
384.904534921278,384.9880881067,385.071685940273,385.155417503134,385.2352513416,
385.318998074302,385.402641751318,385.486202495384,385.569700357341,385.653162857904,
385.736607993396,385.820053828239,385.903518423477,385.987071608899,386.070669442471,
386.154401005333,386.234234843799,386.360598083892,386.415896391545),
 .UNSPECIFIED.);
#475=B_SPLINE_CURVE_WITH_KNOTS('',3,(#59695,#59696,#59697,#59698,#59699,
#59700,#59701,#59702,#59703,#59704,#59705,#59706,#59707,#59708,#59709,#59710,
#59711,#59712,#59713,#59714,#59715,#59716,#59717,#59718,#59719,#59720,#59721,
#59722,#59723,#59724,#59725,#59726,#59727,#59728,#59729,#59730,#59731,#59732,
#59733,#59734,#59735,#59736,#59737,#59738,#59739,#59740,#59741,#59742,#59743,
#59744,#59745,#59746,#59747,#59748,#59749,#59750,#59751,#59752,#59753,#59754,
#59755,#59756,#59757,#59758,#59759,#59760,#59761,#59762,#59763,#59764,#59765,
#59766,#59767,#59768,#59769,#59770,#59771,#59772,#59773,#59774,#59775,#59776,
#59777,#59778,#59779,#59780,#59781,#59782,#59783,#59784,#59785,#59786,#59787,
#59788,#59789,#59790,#59791,#59792,#59793,#59794,#59795,#59796,#59797,#59798,
#59799,#59800,#59801,#59802,#59803,#59804,#59805,#59806,#59807,#59808,#59809,
#59810,#59811,#59812,#59813,#59814,#59815,#59816,#59817,#59818,#59819,#59820,
#59821,#59822,#59823,#59824,#59825,#59826,#59827,#59828,#59829,#59830,#59831,
#59832,#59833,#59834,#59835,#59836,#59837,#59838,#59839,#59840,#59841,#59842,
#59843,#59844,#59845,#59846,#59847,#59848,#59849,#59850,#59851,#59852,#59853,
#59854,#59855,#59856,#59857,#59858,#59859,#59860,#59861,#59862,#59863,#59864,
#59865,#59866,#59867,#59868,#59869,#59870,#59871,#59872,#59873,#59874,#59875,
#59876,#59877,#59878,#59879,#59880,#59881,#59882,#59883,#59884,#59885,#59886,
#59887,#59888,#59889,#59890,#59891,#59892,#59893,#59894,#59895,#59896,#59897,
#59898,#59899,#59900,#59901,#59902,#59903,#59904,#59905,#59906,#59907,#59908,
#59909,#59910,#59911,#59912,#59913,#59914,#59915,#59916,#59917,#59918,#59919,
#59920,#59921,#59922,#59923),.UNSPECIFIED.,.F.,.F.,(4,3,3,3,3,3,3,3,3,3,
3,3,3,3,3,3,3,3,3,3,3,3,3,3,3,3,3,3,3,3,3,3,3,3,3,3,3,3,3,3,3,3,3,3,3,3,
3,3,3,3,3,3,3,3,3,3,3,3,3,3,3,3,3,3,3,3,3,3,3,3,3,3,3,3,3,3,4),(386.415896391695,
386.498269229996,386.580568110831,386.662817848132,386.745042157778,386.827260070869,
386.909490611058,386.991802728423,387.074155810137,387.156638349575,387.233218345998,
387.3169650787,387.400608755716,387.484169499782,387.567667361739,387.651129862302,
387.734574997794,387.818020832637,387.901485427875,387.985038613297,388.068636446869,
388.152368009731,388.232201848197,388.315948580899,388.399592257915,388.483153001981,
388.566650863938,388.650113364501,388.733558499993,388.817004334836,388.900468930075,
388.984022115496,389.067619949069,389.151351511931,389.231185350397,389.314932083099,
389.398575760115,389.482136504181,389.565634366138,389.6490968667,389.732542002193,
389.815987837035,389.899452432273,389.983005617695,390.066603451268,390.15033501413,
390.230168852596,390.313915585298,390.397559262314,390.48112000638,390.564617868337,
390.6480803689,390.731525504392,390.814971339235,390.898435934473,390.981989119895,
391.065586953468,391.14931851633,391.229152354795,391.312899087497,391.396542764513,
391.480103508579,391.563601370536,391.647063871099,391.730509006591,391.813954841434,
391.897419436672,391.980972622094,392.064570455667,392.148302018529,392.228135856994,
392.317403491653,392.406498888698,392.495356687292,392.584067633296,392.672582033764,
392.699081698604),.UNSPECIFIED.);
#476=B_SPLINE_CURVE_WITH_KNOTS('',3,(#59925,#59926,#59927,#59928,#59929,
#59930,#59931,#59932,#59933,#59934,#59935,#59936,#59937,#59938,#59939,#59940,
#59941,#59942,#59943,#59944,#59945,#59946,#59947,#59948,#59949,#59950,#59951,
#59952,#59953,#59954,#59955,#59956,#59957,#59958,#59959,#59960,#59961,#59962,
#59963,#59964,#59965,#59966,#59967,#59968,#59969,#59970,#59971,#59972,#59973,
#59974,#59975,#59976,#59977,#59978,#59979,#59980,#59981,#59982,#59983,#59984,
#59985,#59986,#59987,#59988,#59989,#59990,#59991,#59992,#59993,#59994,#59995,
#59996,#59997,#59998,#59999,#60000,#60001,#60002,#60003,#60004,#60005,#60006,
#60007,#60008,#60009,#60010,#60011,#60012,#60013,#60014,#60015,#60016,#60017,
#60018,#60019,#60020,#60021,#60022,#60023,#60024,#60025,#60026,#60027,#60028,
#60029,#60030,#60031,#60032,#60033,#60034,#60035,#60036,#60037,#60038,#60039,
#60040,#60041,#60042,#60043,#60044,#60045,#60046,#60047,#60048,#60049,#60050,
#60051,#60052,#60053,#60054,#60055,#60056,#60057,#60058,#60059,#60060,#60061,
#60062,#60063,#60064,#60065,#60066,#60067,#60068,#60069,#60070,#60071,#60072,
#60073,#60074,#60075,#60076,#60077,#60078,#60079,#60080,#60081,#60082,#60083,
#60084,#60085,#60086,#60087,#60088,#60089,#60090,#60091,#60092,#60093,#60094,
#60095,#60096,#60097,#60098,#60099,#60100,#60101,#60102,#60103,#60104,#60105,
#60106,#60107,#60108,#60109,#60110,#60111,#60112,#60113,#60114,#60115,#60116,
#60117,#60118,#60119,#60120,#60121,#60122,#60123,#60124,#60125,#60126,#60127,
#60128,#60129,#60130,#60131,#60132,#60133,#60134,#60135,#60136,#60137,#60138,
#60139,#60140,#60141,#60142,#60143,#60144,#60145,#60146,#60147,#60148,#60149,
#60150,#60151,#60152,#60153),.UNSPECIFIED.,.F.,.F.,(4,3,3,3,3,3,3,3,3,3,
3,3,3,3,3,3,3,3,3,3,3,3,3,3,3,3,3,3,3,3,3,3,3,3,3,3,3,3,3,3,3,3,3,3,3,3,
3,3,3,3,3,3,3,3,3,3,3,3,3,3,3,3,3,3,3,3,3,3,3,3,3,3,3,3,3,3,4),(392.699081698725,
392.785525392672,392.872050012387,392.960817349088,393.04760284035,393.137361099771,
393.227119359193,393.310866091895,393.394509768911,393.478070512978,393.561568374935,
393.645030875497,393.72847601099,393.811921845832,393.895386441071,393.978939626492,
394.062537460065,394.146269022927,394.226102861392,394.309849594094,394.39349327111,
394.477054015177,394.560551877134,394.644014377697,394.727459513189,394.810905348032,
394.89436994327,394.977923128692,395.061520962265,395.145252525127,395.225086363592,
395.308833096294,395.39247677331,395.476037517376,395.559535379333,395.642997879896,
395.726443015388,395.809888850231,395.893353445469,395.976906630891,396.060504464463,
396.144236027325,396.224069865791,396.307816598493,396.391460275509,396.475021019575,
396.558518881532,396.641981382094,396.725426517586,396.808872352429,396.892336947667,
396.975890133089,397.059487966661,397.143219529523,397.22305336799,397.306800100692,
397.390443777708,397.474004521774,397.557502383731,397.640964884294,397.724410019786,
397.807855854629,397.891320449867,397.974873635289,398.058471468862,398.142203031724,
398.222036870189,398.304753588746,398.389442765891,398.471956246877,398.554415754322,
398.636840229104,398.723196923304,398.805631483041,398.888083458935,398.970595974559,
398.982267005904),.UNSPECIFIED.);
#477=B_SPLINE_CURVE_WITH_KNOTS('',3,(#60155,#60156,#60157,#60158,#60159,
#60160,#60161,#60162,#60163,#60164,#60165,#60166,#60167,#60168,#60169,#60170,
#60171,#60172,#60173,#60174,#60175,#60176,#60177,#60178,#60179,#60180,#60181,
#60182,#60183,#60184,#60185,#60186,#60187,#60188,#60189,#60190,#60191,#60192,
#60193,#60194,#60195,#60196,#60197,#60198,#60199,#60200,#60201,#60202,#60203,
#60204,#60205,#60206,#60207,#60208,#60209,#60210,#60211,#60212,#60213,#60214,
#60215,#60216,#60217,#60218,#60219,#60220,#60221,#60222,#60223,#60224,#60225,
#60226,#60227,#60228,#60229,#60230,#60231,#60232,#60233,#60234,#60235,#60236,
#60237,#60238,#60239,#60240,#60241,#60242,#60243,#60244,#60245,#60246,#60247,
#60248,#60249,#60250,#60251,#60252,#60253,#60254,#60255,#60256,#60257,#60258,
#60259,#60260,#60261,#60262,#60263,#60264,#60265,#60266,#60267,#60268,#60269,
#60270,#60271,#60272,#60273,#60274,#60275,#60276,#60277,#60278,#60279,#60280,
#60281,#60282,#60283,#60284,#60285,#60286,#60287,#60288,#60289,#60290,#60291,
#60292,#60293,#60294,#60295,#60296,#60297,#60298,#60299,#60300,#60301,#60302,
#60303,#60304,#60305,#60306,#60307,#60308,#60309,#60310,#60311,#60312,#60313,
#60314,#60315,#60316,#60317,#60318,#60319,#60320,#60321,#60322,#60323,#60324,
#60325,#60326,#60327,#60328,#60329,#60330,#60331,#60332,#60333,#60334,#60335,
#60336,#60337,#60338,#60339,#60340,#60341,#60342,#60343,#60344,#60345,#60346,
#60347,#60348,#60349,#60350,#60351,#60352,#60353,#60354,#60355,#60356,#60357,
#60358,#60359,#60360,#60361,#60362,#60363,#60364,#60365,#60366,#60367,#60368,
#60369,#60370,#60371,#60372,#60373,#60374,#60375,#60376,#60377,#60378,#60379,
#60380,#60381,#60382,#60383),.UNSPECIFIED.,.F.,.F.,(4,3,3,3,3,3,3,3,3,3,
3,3,3,3,3,3,3,3,3,3,3,3,3,3,3,3,3,3,3,3,3,3,3,3,3,3,3,3,3,3,3,3,3,3,3,3,
3,3,3,3,3,3,3,3,3,3,3,3,3,3,3,3,3,3,3,3,3,3,3,3,3,3,3,3,3,3,4),(398.982267006032,
399.091341048604,399.203228576954,399.221020372388,399.30476710509,399.388410782106,
399.471971526173,399.555469388129,399.638931888692,399.722377024185,399.805822859028,
399.889287454266,399.972840639688,400.05643847326,400.140170036122,400.220003874587,
400.303750607289,400.387394284305,400.470955028371,400.554452890328,400.637915390891,
400.721360526383,400.804806361226,400.888270956464,400.971824141886,401.055421975458,
401.13915353832,401.218987376787,401.302734109489,401.386377786505,401.469938530572,
401.553436392528,401.636898893091,401.720344028583,401.803789863426,401.887254458664,
401.970807644086,402.054405477659,402.138137040521,402.217970878986,402.301717611688,
402.385361288704,402.46892203277,402.552419894727,402.635882395289,402.719327530782,
402.802773365624,402.886237960862,402.969791146284,403.053388979857,403.137120542718,
403.216954381185,403.300701113887,403.384344790903,403.467905534969,403.551403396926,
403.634865897489,403.718311032981,403.801756867824,403.885221463062,403.968774648484,
404.052372482056,404.136104044918,404.215937883384,404.299684616086,404.383328293102,
404.466889037168,404.550386899125,404.633849399687,404.71729453518,404.800740370022,
404.88420496526,404.967758150682,405.051355984255,405.135087547117,405.214921385583,
405.265452313084),.UNSPECIFIED.);
#478=B_SPLINE_CURVE_WITH_KNOTS('',3,(#60385,#60386,#60387,#60388,#60389,
#60390,#60391,#60392,#60393,#60394,#60395,#60396,#60397,#60398,#60399,#60400,
#60401,#60402,#60403,#60404,#60405,#60406,#60407,#60408,#60409,#60410,#60411,
#60412,#60413,#60414,#60415,#60416,#60417,#60418,#60419,#60420,#60421,#60422,
#60423,#60424,#60425,#60426,#60427,#60428,#60429,#60430,#60431,#60432,#60433,
#60434,#60435,#60436,#60437,#60438,#60439,#60440,#60441,#60442,#60443,#60444,
#60445,#60446,#60447,#60448,#60449,#60450,#60451,#60452,#60453,#60454,#60455,
#60456,#60457,#60458,#60459,#60460,#60461,#60462,#60463,#60464,#60465,#60466,
#60467,#60468,#60469,#60470,#60471,#60472,#60473,#60474,#60475,#60476,#60477,
#60478,#60479,#60480,#60481,#60482,#60483,#60484,#60485,#60486,#60487,#60488,
#60489,#60490,#60491,#60492,#60493,#60494,#60495,#60496,#60497,#60498,#60499,
#60500,#60501,#60502,#60503,#60504,#60505,#60506,#60507,#60508,#60509,#60510,
#60511,#60512,#60513,#60514,#60515,#60516,#60517,#60518,#60519,#60520,#60521,
#60522,#60523,#60524,#60525,#60526,#60527,#60528,#60529,#60530,#60531,#60532,
#60533,#60534,#60535,#60536,#60537,#60538,#60539,#60540,#60541,#60542,#60543,
#60544,#60545,#60546,#60547,#60548,#60549,#60550,#60551,#60552,#60553,#60554,
#60555,#60556,#60557,#60558,#60559,#60560,#60561,#60562,#60563,#60564,#60565,
#60566,#60567,#60568,#60569,#60570,#60571,#60572,#60573,#60574,#60575,#60576,
#60577,#60578,#60579,#60580,#60581,#60582,#60583,#60584,#60585,#60586,#60587,
#60588,#60589,#60590,#60591,#60592,#60593,#60594,#60595,#60596,#60597,#60598,
#60599,#60600,#60601,#60602,#60603,#60604,#60605,#60606,#60607,#60608,#60609,
#60610,#60611,#60612,#60613),.UNSPECIFIED.,.F.,.F.,(4,3,3,3,3,3,3,3,3,3,
3,3,3,3,3,3,3,3,3,3,3,3,3,3,3,3,3,3,3,3,3,3,3,3,3,3,3,3,3,3,3,3,3,3,3,3,
3,3,3,3,3,3,3,3,3,3,3,3,3,3,3,3,3,3,3,3,3,3,3,3,3,3,3,3,3,3,4),(405.265452313283,
405.348538923691,405.431525689357,405.514433352743,405.597282579425,405.680102760379,
405.762910725424,405.845725095357,405.928564492279,406.011493653704,406.094474155631,
406.177574913904,406.213904887782,406.297651620484,406.3812952975,406.464856041566,
406.548353903523,406.631816404086,406.715261539578,406.798707374421,406.882171969659,
406.965725155081,407.049322988654,407.133054551516,407.212888389982,407.296635122684,
407.3802787997,407.463839543766,407.547337405723,407.630799906285,407.714245041778,
407.797690876621,407.881155471859,407.964708657281,408.048306490853,408.132038053715,
408.211871892181,408.295618624883,408.379262301899,408.462823045965,408.546320907922,
408.629783408484,408.713228543977,408.796674378819,408.880138974057,408.963692159479,
409.047289993052,409.131021555914,409.21085539438,409.294602127082,409.378245804098,
409.461806548164,409.545304410121,409.628766910684,409.712212046176,409.795657881019,
409.879122476257,409.962675661679,410.046273495252,410.130005058113,410.209838896579,
410.293585629281,410.377229306297,410.460790050363,410.54428791232,410.627750412883,
410.711195548375,410.794641383218,410.878105978456,410.961659163878,411.04525699745,
411.128988560312,411.208822398778,411.306570851759,411.403897232893,411.500435641759,
411.548637620263),.UNSPECIFIED.);
#479=B_SPLINE_CURVE_WITH_KNOTS('',3,(#60615,#60616,#60617,#60618,#60619,
#60620,#60621,#60622,#60623,#60624),.UNSPECIFIED.,.F.,.F.,(4,1,1,1,1,1,
1,4),(411.548637620263,412.207805900977,413.206789403177,414.205772905376,
415.204756407575,416.203739909774,417.202723411973,417.831822927443),
 .UNSPECIFIED.);
#480=B_SPLINE_CURVE_WITH_KNOTS('',3,(#60626,#60627,#60628,#60629,#60630,
#60631,#60632,#60633,#60634,#60635,#60636,#60637,#60638,#60639,#60640,#60641,
#60642,#60643,#60644,#60645,#60646,#60647,#60648,#60649,#60650,#60651,#60652,
#60653,#60654,#60655,#60656,#60657,#60658,#60659,#60660,#60661,#60662,#60663,
#60664,#60665,#60666,#60667,#60668,#60669,#60670,#60671,#60672,#60673,#60674,
#60675,#60676,#60677,#60678,#60679,#60680,#60681,#60682,#60683,#60684,#60685,
#60686,#60687,#60688,#60689,#60690,#60691,#60692,#60693,#60694,#60695,#60696,
#60697,#60698,#60699,#60700,#60701,#60702,#60703,#60704,#60705,#60706,#60707,
#60708,#60709,#60710,#60711,#60712,#60713,#60714,#60715,#60716,#60717,#60718,
#60719,#60720,#60721,#60722,#60723,#60724,#60725,#60726,#60727,#60728,#60729,
#60730,#60731,#60732,#60733,#60734,#60735,#60736,#60737,#60738,#60739,#60740,
#60741,#60742,#60743,#60744,#60745,#60746,#60747,#60748,#60749,#60750,#60751,
#60752,#60753,#60754,#60755,#60756,#60757,#60758,#60759,#60760,#60761,#60762,
#60763,#60764,#60765,#60766,#60767,#60768,#60769,#60770,#60771,#60772,#60773,
#60774,#60775,#60776,#60777,#60778,#60779,#60780,#60781,#60782,#60783,#60784,
#60785,#60786,#60787,#60788,#60789,#60790,#60791,#60792,#60793,#60794,#60795,
#60796,#60797,#60798,#60799,#60800,#60801,#60802,#60803,#60804,#60805,#60806,
#60807,#60808,#60809,#60810,#60811,#60812,#60813,#60814,#60815,#60816,#60817,
#60818,#60819,#60820,#60821,#60822,#60823,#60824,#60825,#60826,#60827,#60828,
#60829,#60830,#60831,#60832,#60833,#60834,#60835,#60836,#60837,#60838,#60839,
#60840,#60841,#60842,#60843,#60844,#60845,#60846,#60847,#60848,#60849,#60850,
#60851),.UNSPECIFIED.,.F.,.F.,(4,3,3,3,3,3,3,3,3,3,3,3,3,3,3,3,3,3,3,3,
3,3,3,3,3,3,3,3,3,3,3,3,3,3,3,3,3,3,3,3,3,3,3,3,3,3,3,3,3,3,3,3,3,3,3,3,
3,3,3,3,3,3,3,3,3,3,3,3,3,3,3,3,3,3,3,4),(417.831822927443,417.926099988475,
418.020755754091,418.115941577717,418.201706914172,418.285453646874,418.36909732389,
418.452658067957,418.536155929914,418.619618430476,418.703063565969,418.786509400811,
418.869973996049,418.953527181471,419.037125015044,419.120856577906,419.200690416372,
419.284437149074,419.36808082609,419.451641570156,419.535139432113,419.618601932676,
419.702047068168,419.785492903011,419.868957498249,419.952510683671,420.036108517243,
420.119840080105,420.199673918571,420.283420651273,420.367064328289,420.450625072355,
420.534122934312,420.617585434875,420.701030570367,420.78447640521,420.867941000448,
420.95149418587,421.035092019442,421.118823582304,421.19865742077,421.282404153472,
421.366047830488,421.449608574554,421.533106436511,421.616568937073,421.700014072566,
421.783459907408,421.866924502646,421.950477688068,422.034075521641,422.117807084503,
422.197640922969,422.281387655671,422.365031332687,422.448592076753,422.53208993871,
422.615552439273,422.698997574765,422.782443409608,422.865908004846,422.949461190268,
423.03305902384,423.116790586702,423.196624425168,423.27945481212,423.362182857043,
423.444829539153,423.52860187607,423.611154980827,423.693694510841,423.776239281408,
423.86093151968,423.94358394385,424.029296089172,424.115008234493),
 .UNSPECIFIED.);
#481=B_SPLINE_CURVE_WITH_KNOTS('',3,(#60853,#60854,#60855,#60856,#60857,
#60858,#60859,#60860,#60861,#60862,#60863,#60864,#60865,#60866,#60867,#60868,
#60869,#60870,#60871,#60872,#60873,#60874,#60875,#60876,#60877,#60878,#60879,
#60880,#60881,#60882,#60883,#60884,#60885,#60886,#60887,#60888,#60889,#60890,
#60891,#60892,#60893,#60894,#60895,#60896,#60897,#60898,#60899,#60900,#60901,
#60902,#60903,#60904,#60905,#60906,#60907,#60908,#60909,#60910,#60911,#60912,
#60913,#60914,#60915,#60916,#60917,#60918,#60919,#60920,#60921,#60922,#60923,
#60924,#60925,#60926,#60927,#60928,#60929,#60930,#60931,#60932,#60933,#60934,
#60935,#60936,#60937,#60938,#60939,#60940,#60941,#60942,#60943,#60944,#60945,
#60946,#60947,#60948,#60949,#60950,#60951,#60952,#60953,#60954,#60955,#60956,
#60957,#60958,#60959,#60960,#60961,#60962,#60963,#60964,#60965,#60966,#60967,
#60968,#60969,#60970,#60971,#60972,#60973,#60974,#60975,#60976,#60977,#60978,
#60979,#60980,#60981,#60982,#60983,#60984,#60985,#60986,#60987,#60988,#60989,
#60990,#60991,#60992,#60993,#60994,#60995,#60996,#60997,#60998,#60999,#61000,
#61001,#61002,#61003,#61004,#61005,#61006,#61007,#61008,#61009,#61010,#61011,
#61012,#61013,#61014,#61015,#61016,#61017,#61018,#61019,#61020,#61021,#61022,
#61023,#61024,#61025,#61026,#61027,#61028,#61029,#61030,#61031,#61032,#61033,
#61034,#61035,#61036,#61037,#61038,#61039,#61040,#61041,#61042,#61043,#61044,
#61045,#61046,#61047,#61048,#61049,#61050,#61051,#61052,#61053,#61054,#61055,
#61056,#61057,#61058,#61059,#61060,#61061,#61062,#61063,#61064,#61065,#61066,
#61067,#61068,#61069,#61070,#61071,#61072,#61073,#61074,#61075,#61076,#61077,
#61078),.UNSPECIFIED.,.F.,.F.,(4,3,3,3,3,3,3,3,3,3,3,3,3,3,3,3,3,3,3,3,
3,3,3,3,3,3,3,3,3,3,3,3,3,3,3,3,3,3,3,3,3,3,3,3,3,3,3,3,3,3,3,3,3,3,3,3,
3,3,3,3,3,3,3,3,3,3,3,3,3,3,3,3,3,3,3,4),(424.115008234623,424.195607927367,
424.279354660069,424.362998337085,424.446559081151,424.530056943108,424.61351944367,
424.696964579163,424.780410414005,424.863875009243,424.947428194665,425.031026028238,
425.1147575911,425.194591429567,425.278338162269,425.361981839285,425.445542583352,
425.529040445308,425.612502945871,425.695948081363,425.779393916206,425.862858511444,
425.946411696866,426.030009530439,426.113741093301,426.193574931766,426.277321664468,
426.360965341484,426.44452608555,426.528023947507,426.61148644807,426.694931583562,
426.778377418405,426.861842013643,426.945395199064,427.028993032637,427.112724595499,
427.192558433965,427.276305166667,427.359948843683,427.443509587749,427.527007449706,
427.610469950269,427.693915085761,427.777360920604,427.860825515842,427.944378701264,
428.027976534836,428.111708097698,428.191541936164,428.275288668866,428.358932345882,
428.442493089948,428.525990951905,428.609453452467,428.69289858796,428.776344422802,
428.85980901804,428.943362203462,429.026960037035,429.110691599897,429.190525438363,
429.274272171065,429.357915848081,429.441476592147,429.524974454104,429.608436954667,
429.691882090159,429.775327925002,429.85879252024,429.942345705662,430.025943539235,
430.109675102096,430.189508940562,430.307067979204,430.398193541802),
 .UNSPECIFIED.);
#482=B_SPLINE_CURVE_WITH_KNOTS('',3,(#61080,#61081,#61082,#61083,#61084,
#61085,#61086,#61087,#61088,#61089,#61090,#61091,#61092,#61093,#61094,#61095,
#61096,#61097,#61098,#61099,#61100,#61101,#61102,#61103,#61104,#61105,#61106,
#61107,#61108,#61109,#61110,#61111,#61112,#61113,#61114,#61115,#61116,#61117,
#61118,#61119,#61120,#61121,#61122,#61123,#61124,#61125,#61126,#61127,#61128,
#61129,#61130,#61131,#61132,#61133,#61134,#61135,#61136,#61137,#61138,#61139,
#61140,#61141,#61142,#61143,#61144,#61145,#61146,#61147,#61148,#61149,#61150,
#61151,#61152,#61153,#61154,#61155,#61156,#61157,#61158,#61159,#61160,#61161,
#61162,#61163,#61164,#61165,#61166,#61167,#61168,#61169,#61170,#61171,#61172,
#61173,#61174,#61175,#61176,#61177,#61178,#61179,#61180,#61181,#61182,#61183,
#61184,#61185,#61186,#61187,#61188,#61189,#61190,#61191,#61192,#61193,#61194,
#61195,#61196,#61197,#61198,#61199,#61200,#61201,#61202,#61203,#61204,#61205,
#61206,#61207,#61208,#61209,#61210,#61211,#61212,#61213,#61214,#61215,#61216,
#61217,#61218,#61219,#61220,#61221,#61222,#61223,#61224,#61225,#61226,#61227,
#61228,#61229,#61230,#61231,#61232,#61233,#61234,#61235,#61236,#61237,#61238,
#61239,#61240,#61241,#61242,#61243,#61244,#61245,#61246,#61247,#61248,#61249,
#61250,#61251,#61252,#61253,#61254,#61255,#61256,#61257,#61258,#61259,#61260,
#61261,#61262,#61263,#61264,#61265,#61266,#61267,#61268,#61269,#61270,#61271,
#61272,#61273,#61274,#61275,#61276,#61277,#61278,#61279,#61280,#61281,#61282,
#61283,#61284,#61285,#61286,#61287,#61288,#61289,#61290,#61291,#61292,#61293,
#61294,#61295,#61296,#61297,#61298,#61299,#61300,#61301,#61302,#61303,#61304,
#61305,#61306,#61307,#61308),.UNSPECIFIED.,.F.,.F.,(4,3,3,3,3,3,3,3,3,3,
3,3,3,3,3,3,3,3,3,3,3,3,3,3,3,3,3,3,3,3,3,3,3,3,3,3,3,3,3,3,3,3,3,3,3,3,
3,3,3,3,3,3,3,3,3,3,3,3,3,3,3,3,3,3,3,3,3,3,3,3,3,3,3,3,3,3,4),(430.398193541946,
430.480597550544,430.562935285471,430.645234069969,430.72751428009,430.809794904858,
430.892094931353,430.974480349292,431.056912748385,431.139467268808,431.188492442761,
431.272239175463,431.355882852479,431.439443596545,431.522941458502,431.606403959065,
431.689849094557,431.7732949294,431.856759524638,431.94031271006,432.023910543632,
432.107642106494,432.187475944961,432.271222677663,432.354866354679,432.438427098745,
432.521924960702,432.605387461264,432.688832596757,432.7722784316,432.855743026838,
432.93929621226,433.022894045833,433.106625608695,433.18645944716,433.270206179862,
433.353849856878,433.437410600944,433.5209084629,433.604370963463,433.687816098955,
433.771261933798,433.854726529036,433.938279714458,434.021877548031,434.105609110892,
434.185442949359,434.269189682061,434.352833359077,434.436394103143,434.5198919651,
434.603354465662,434.686799601155,434.770245435998,434.853710031236,434.937263216658,
435.02086105023,435.104592613092,435.184426451558,435.26817318426,435.351816861276,
435.435377605342,435.518875467299,435.602337967861,435.685783103354,435.769228938196,
435.852693533434,435.936246718856,436.019844552429,436.10357611529,436.183409953757,
436.271527674377,436.359492756615,436.447255588697,436.534897976604,436.622381849063,
436.681378848596),.UNSPECIFIED.);
#483=B_SPLINE_CURVE_WITH_KNOTS('',3,(#61310,#61311,#61312,#61313,#61314,
#61315,#61316,#61317,#61318,#61319,#61320,#61321,#61322,#61323,#61324,#61325,
#61326,#61327,#61328,#61329,#61330,#61331,#61332,#61333,#61334,#61335,#61336,
#61337,#61338,#61339,#61340,#61341,#61342,#61343,#61344,#61345,#61346,#61347,
#61348,#61349,#61350,#61351,#61352,#61353,#61354,#61355,#61356,#61357,#61358,
#61359,#61360,#61361,#61362,#61363,#61364,#61365,#61366,#61367,#61368,#61369,
#61370,#61371,#61372,#61373,#61374,#61375,#61376,#61377,#61378,#61379,#61380,
#61381,#61382,#61383,#61384,#61385,#61386,#61387,#61388,#61389,#61390,#61391,
#61392,#61393,#61394,#61395,#61396,#61397,#61398,#61399,#61400,#61401,#61402,
#61403,#61404,#61405,#61406,#61407,#61408,#61409,#61410,#61411,#61412,#61413,
#61414,#61415,#61416,#61417,#61418,#61419,#61420,#61421,#61422,#61423,#61424,
#61425,#61426,#61427,#61428,#61429,#61430,#61431,#61432,#61433,#61434,#61435,
#61436,#61437,#61438,#61439,#61440,#61441,#61442,#61443,#61444,#61445,#61446,
#61447,#61448,#61449,#61450,#61451,#61452,#61453,#61454,#61455,#61456,#61457,
#61458,#61459,#61460,#61461,#61462,#61463,#61464,#61465,#61466,#61467,#61468,
#61469,#61470,#61471,#61472,#61473,#61474,#61475,#61476,#61477,#61478,#61479,
#61480,#61481,#61482,#61483,#61484,#61485,#61486,#61487,#61488,#61489,#61490,
#61491,#61492,#61493,#61494,#61495,#61496,#61497,#61498,#61499,#61500,#61501,
#61502,#61503,#61504,#61505,#61506,#61507,#61508,#61509,#61510,#61511,#61512,
#61513,#61514,#61515,#61516,#61517,#61518,#61519,#61520,#61521,#61522,#61523,
#61524,#61525,#61526,#61527,#61528,#61529,#61530,#61531,#61532,#61533,#61534,
#61535,#61536,#61537,#61538),.UNSPECIFIED.,.F.,.F.,(4,3,3,3,3,3,3,3,3,3,
3,3,3,3,3,3,3,3,3,3,3,3,3,3,3,3,3,3,3,3,3,3,3,3,3,3,3,3,3,3,3,3,3,3,3,3,
3,3,3,3,3,3,3,3,3,3,3,3,3,3,3,3,3,3,3,3,3,3,3,3,3,3,3,3,3,3,4),(436.681378848982,
436.768731500326,436.856196957168,436.943866686287,437.031644010499,437.119621670839,
437.182393455956,437.266140188658,437.349783865674,437.43334460974,437.516842471697,
437.60030497226,437.683750107752,437.767195942595,437.850660537833,437.934213723255,
438.017811556828,438.10154311969,438.181376958156,438.265123690858,438.348767367874,
438.432328111941,438.515825973897,438.59928847446,438.682733609952,438.766179444795,
438.849644040033,438.933197225455,439.016795059028,439.10052662189,439.180360460355,
439.264107193057,439.347750870073,439.431311614139,439.514809476096,439.598271976659,
439.681717112151,439.765162946994,439.848627542231,439.932180727653,440.015778561226,
440.099510124088,440.179343962554,440.263090695256,440.346734372272,440.430295116338,
440.513792978295,440.597255478857,440.68070061435,440.764146449192,440.84761104443,
440.931164229852,441.014762063425,441.098493626287,441.178327464753,441.262074197455,
441.345717874471,441.429278618538,441.512776480494,441.596238981057,441.679684116549,
441.763129951392,441.84659454663,441.930147732052,442.013745565625,442.097477128487,
442.177310966952,442.259891588733,442.342368707561,442.424750977318,442.507080149116,
442.589375248686,442.671655270268,442.753967832792,442.836297761573,442.918702822903,
442.964564156035),.UNSPECIFIED.);
#484=B_SPLINE_CURVE_WITH_KNOTS('',3,(#61540,#61541,#61542,#61543,#61544,
#61545,#61546,#61547,#61548,#61549,#61550,#61551,#61552,#61553,#61554,#61555,
#61556,#61557,#61558,#61559,#61560,#61561,#61562,#61563,#61564,#61565,#61566,
#61567,#61568,#61569,#61570,#61571,#61572,#61573,#61574,#61575,#61576,#61577,
#61578,#61579,#61580,#61581,#61582,#61583,#61584,#61585,#61586,#61587,#61588,
#61589,#61590,#61591,#61592,#61593,#61594,#61595,#61596,#61597,#61598,#61599,
#61600,#61601,#61602,#61603,#61604,#61605,#61606,#61607,#61608,#61609,#61610,
#61611,#61612,#61613,#61614,#61615,#61616,#61617,#61618,#61619,#61620,#61621,
#61622,#61623,#61624,#61625,#61626,#61627,#61628,#61629,#61630,#61631,#61632,
#61633,#61634,#61635,#61636,#61637,#61638,#61639,#61640,#61641,#61642,#61643,
#61644,#61645,#61646,#61647,#61648,#61649,#61650,#61651,#61652,#61653,#61654,
#61655,#61656,#61657,#61658,#61659,#61660,#61661,#61662,#61663,#61664,#61665,
#61666,#61667,#61668,#61669,#61670,#61671,#61672,#61673,#61674,#61675,#61676,
#61677,#61678,#61679,#61680,#61681,#61682,#61683,#61684,#61685,#61686,#61687,
#61688,#61689,#61690,#61691,#61692,#61693,#61694,#61695,#61696,#61697,#61698,
#61699,#61700,#61701,#61702,#61703,#61704,#61705,#61706,#61707,#61708,#61709,
#61710,#61711,#61712,#61713,#61714,#61715,#61716,#61717,#61718,#61719,#61720,
#61721,#61722,#61723,#61724,#61725,#61726,#61727,#61728,#61729,#61730,#61731,
#61732,#61733,#61734,#61735,#61736,#61737,#61738,#61739,#61740,#61741,#61742,
#61743,#61744,#61745,#61746,#61747,#61748,#61749,#61750,#61751,#61752,#61753,
#61754,#61755,#61756,#61757,#61758,#61759,#61760,#61761,#61762,#61763,#61764,
#61765),.UNSPECIFIED.,.F.,.F.,(4,3,3,3,3,3,3,3,3,3,3,3,3,3,3,3,3,3,3,3,
3,3,3,3,3,3,3,3,3,3,3,3,3,3,3,3,3,3,3,3,3,3,3,3,3,3,3,3,3,3,3,3,3,3,3,3,
3,3,3,3,3,3,3,3,3,3,3,3,3,3,3,3,3,3,3,4),(442.964564156161,443.081306905342,
443.176294469151,443.260041201853,443.343684878869,443.427245622936,443.510743484892,
443.594205985455,443.677651120947,443.76109695579,443.844561551028,443.92811473645,
444.011712570023,444.095444132884,444.175277971351,444.259024704053,444.342668381069,
444.426229125136,444.509726987092,444.593189487655,444.676634623147,444.76008045799,
444.843545053228,444.92709823865,445.010696072223,445.094427635084,445.17426147355,
445.258008206252,445.341651883268,445.425212627334,445.508710489291,445.592172989853,
445.675618125346,445.759063960188,445.842528555426,445.926081740848,446.009679574421,
446.093411137283,446.173244975749,446.256991708451,446.340635385467,446.424196129533,
446.50769399149,446.591156492053,446.674601627545,446.758047462388,446.841512057626,
446.925065243048,447.00866307662,447.092394639482,447.172228477948,447.25597521065,
447.339618887666,447.423179631732,447.506677493689,447.590139994252,447.673585129744,
447.757030964587,447.840495559825,447.924048745246,448.007646578819,448.091378141681,
448.171211980147,448.254958712849,448.338602389865,448.422163133931,448.505660995888,
448.58912349645,448.672568631943,448.756014466786,448.839479062024,448.923032247446,
449.006630081018,449.09036164388,449.170195482346,449.247749463341),
 .UNSPECIFIED.);
#485=B_SPLINE_CURVE_WITH_KNOTS('',3,(#61767,#61768,#61769,#61770,#61771,
#61772,#61773,#61774,#61775,#61776,#61777,#61778,#61779,#61780,#61781,#61782,
#61783,#61784,#61785,#61786,#61787,#61788,#61789,#61790,#61791,#61792,#61793,
#61794,#61795,#61796,#61797,#61798,#61799,#61800,#61801,#61802,#61803,#61804,
#61805,#61806,#61807,#61808,#61809,#61810,#61811,#61812,#61813,#61814,#61815,
#61816,#61817,#61818,#61819,#61820,#61821,#61822,#61823,#61824,#61825,#61826,
#61827,#61828,#61829,#61830,#61831,#61832,#61833,#61834,#61835,#61836,#61837,
#61838,#61839,#61840,#61841,#61842,#61843,#61844,#61845,#61846,#61847,#61848,
#61849,#61850,#61851,#61852,#61853,#61854,#61855,#61856,#61857,#61858,#61859,
#61860,#61861,#61862,#61863,#61864,#61865,#61866,#61867,#61868,#61869,#61870,
#61871,#61872,#61873,#61874,#61875,#61876,#61877,#61878,#61879,#61880,#61881,
#61882,#61883,#61884,#61885,#61886,#61887,#61888,#61889,#61890,#61891,#61892,
#61893,#61894,#61895,#61896,#61897,#61898,#61899,#61900,#61901,#61902,#61903,
#61904,#61905,#61906,#61907,#61908,#61909,#61910,#61911,#61912,#61913,#61914,
#61915,#61916,#61917,#61918,#61919,#61920,#61921,#61922,#61923,#61924,#61925,
#61926,#61927,#61928,#61929,#61930,#61931,#61932,#61933,#61934,#61935,#61936,
#61937,#61938,#61939,#61940,#61941,#61942,#61943,#61944,#61945,#61946,#61947,
#61948,#61949,#61950,#61951,#61952,#61953,#61954,#61955,#61956,#61957,#61958,
#61959,#61960,#61961,#61962,#61963,#61964,#61965,#61966,#61967,#61968,#61969,
#61970,#61971,#61972,#61973,#61974,#61975,#61976,#61977,#61978,#61979,#61980,
#61981,#61982,#61983,#61984,#61985,#61986,#61987,#61988,#61989,#61990,#61991,
#61992),.UNSPECIFIED.,.F.,.F.,(4,3,3,3,3,3,3,3,3,3,3,3,3,3,3,3,3,3,3,3,
3,3,3,3,3,3,3,3,3,3,3,3,3,3,3,3,3,3,3,3,3,3,3,3,3,3,3,3,3,3,3,3,3,3,3,3,
3,3,3,3,3,3,3,3,3,3,3,3,3,3,3,3,3,3,3,4),(449.247749463469,449.330572004686,
449.413298292432,449.495949259883,449.580102975466,449.662675299464,449.745239696899,
449.827814966215,449.913155970798,449.995853631113,450.082516307829,450.169178984546,
450.252925717248,450.336569394264,450.42013013833,450.503628000287,450.58709050085,
450.670535636342,450.753981471185,450.837446066423,450.920999251845,451.004597085417,
451.088328648279,451.168162486745,451.251909219447,451.335552896463,451.419113640529,
451.502611502486,451.586074003048,451.669519138541,451.752964973383,451.836429568622,
451.919982754043,452.003580587616,452.087312150478,452.167145988944,452.250892721646,
452.334536398662,452.418097142728,452.501595004685,452.585057505248,452.66850264074,
452.751948475583,452.835413070821,452.918966256243,453.002564089816,453.086295652677,
453.166129491143,453.249876223845,453.333519900861,453.417080644927,453.500578506883,
453.584041007446,453.667486142938,453.750931977781,453.834396573019,453.917949758441,
454.001547592014,454.085279154875,454.165112993342,454.248859726044,454.33250340306,
454.416064147126,454.499562009083,454.583024509646,454.666469645138,454.749915479981,
454.833380075219,454.91693326064,455.000531094213,455.084262657075,455.164096495541,
455.259513492123,455.354608932559,455.449086084506,455.530934770324),
 .UNSPECIFIED.);
#486=B_SPLINE_CURVE_WITH_KNOTS('',3,(#61994,#61995,#61996,#61997,#61998,
#61999,#62000,#62001,#62002,#62003,#62004,#62005,#62006,#62007,#62008,#62009,
#62010,#62011,#62012,#62013,#62014,#62015,#62016,#62017,#62018,#62019,#62020,
#62021,#62022,#62023,#62024,#62025,#62026,#62027,#62028,#62029,#62030,#62031,
#62032,#62033,#62034,#62035,#62036,#62037,#62038,#62039,#62040,#62041,#62042,
#62043,#62044,#62045,#62046,#62047,#62048,#62049,#62050,#62051,#62052,#62053,
#62054,#62055,#62056,#62057,#62058,#62059,#62060,#62061,#62062,#62063,#62064,
#62065,#62066,#62067,#62068,#62069,#62070,#62071,#62072,#62073,#62074,#62075,
#62076,#62077,#62078,#62079,#62080,#62081,#62082,#62083,#62084,#62085,#62086,
#62087,#62088,#62089,#62090,#62091,#62092,#62093,#62094,#62095,#62096,#62097,
#62098,#62099,#62100,#62101,#62102,#62103,#62104,#62105,#62106,#62107,#62108,
#62109,#62110,#62111,#62112,#62113,#62114,#62115,#62116,#62117,#62118,#62119,
#62120,#62121,#62122,#62123,#62124,#62125,#62126,#62127,#62128,#62129,#62130,
#62131,#62132,#62133,#62134,#62135,#62136,#62137,#62138,#62139,#62140,#62141,
#62142,#62143,#62144,#62145,#62146,#62147,#62148,#62149,#62150,#62151,#62152,
#62153,#62154,#62155,#62156,#62157,#62158,#62159,#62160,#62161,#62162,#62163,
#62164,#62165,#62166,#62167,#62168,#62169,#62170,#62171,#62172,#62173,#62174,
#62175,#62176,#62177,#62178,#62179,#62180,#62181,#62182,#62183,#62184,#62185,
#62186,#62187,#62188,#62189,#62190,#62191,#62192,#62193,#62194,#62195,#62196,
#62197,#62198,#62199,#62200,#62201,#62202,#62203,#62204,#62205,#62206,#62207,
#62208,#62209,#62210,#62211,#62212,#62213,#62214,#62215,#62216,#62217,#62218,
#62219,#62220,#62221,#62222),.UNSPECIFIED.,.F.,.F.,(4,3,3,3,3,3,3,3,3,3,
3,3,3,3,3,3,3,3,3,3,3,3,3,3,3,3,3,3,3,3,3,3,3,3,3,3,3,3,3,3,3,3,3,3,3,3,
3,3,3,3,3,3,3,3,3,3,3,3,3,3,3,3,3,3,3,3,3,3,3,3,3,3,3,3,3,3,4),(455.53093477052,
455.614864815332,455.698797940928,455.782751521101,455.866742939129,455.950841680949,
456.035000609231,456.119294244176,456.163079997741,456.246826730443,456.330470407459,
456.414031151525,456.497529013482,456.580991514045,456.664436649537,456.74788248438,
456.831347079618,456.91490026504,456.998498098613,457.082229661475,457.16206349994,
457.245810232642,457.329453909658,457.413014653724,457.496512515681,457.579975016244,
457.663420151736,457.746865986578,457.830330581816,457.913883767238,457.997481600811,
458.081213163673,458.161047002139,458.244793734841,458.328437411857,458.411998155923,
458.49549601788,458.578958518442,458.662403653935,458.745849488777,458.829314084015,
458.912867269437,458.99646510301,459.080196665872,459.160030504338,459.24377723704,
459.327420914056,459.410981658123,459.494479520079,459.577942020642,459.661387156134,
459.744832990977,459.828297586215,459.911850771636,459.995448605209,460.079180168071,
460.159014006537,460.242760739239,460.326404416255,460.409965160321,460.493463022277,
460.57692552284,460.660370658332,460.743816493175,460.827281088413,460.910834273835,
460.994432107408,461.07816367027,461.157997508736,461.241847586848,461.32559581153,
461.40926024753,461.492858897943,461.57641249266,461.659938082167,461.74347381492,
461.8141200777),.UNSPECIFIED.);
#487=B_SPLINE_CURVE_WITH_KNOTS('',3,(#62224,#62225,#62226,#62227,#62228,
#62229,#62230,#62231,#62232,#62233,#62234,#62235,#62236,#62237,#62238,#62239,
#62240,#62241,#62242,#62243,#62244,#62245,#62246,#62247,#62248,#62249,#62250,
#62251,#62252,#62253,#62254,#62255,#62256,#62257,#62258,#62259,#62260,#62261,
#62262,#62263,#62264,#62265,#62266,#62267,#62268,#62269,#62270,#62271,#62272,
#62273,#62274,#62275,#62276,#62277,#62278,#62279,#62280,#62281,#62282,#62283,
#62284,#62285,#62286,#62287,#62288,#62289,#62290,#62291,#62292,#62293,#62294,
#62295,#62296,#62297,#62298,#62299,#62300,#62301,#62302,#62303,#62304,#62305,
#62306,#62307,#62308,#62309,#62310,#62311,#62312,#62313,#62314,#62315,#62316,
#62317,#62318,#62319,#62320,#62321,#62322,#62323,#62324,#62325,#62326,#62327,
#62328,#62329,#62330,#62331,#62332,#62333,#62334,#62335,#62336,#62337,#62338,
#62339,#62340,#62341,#62342,#62343,#62344,#62345,#62346,#62347,#62348,#62349,
#62350,#62351,#62352,#62353,#62354,#62355,#62356,#62357,#62358,#62359,#62360,
#62361,#62362,#62363,#62364,#62365,#62366,#62367,#62368,#62369,#62370,#62371,
#62372,#62373,#62374,#62375,#62376,#62377,#62378,#62379,#62380,#62381,#62382,
#62383,#62384,#62385,#62386,#62387,#62388,#62389,#62390,#62391,#62392,#62393,
#62394,#62395,#62396,#62397,#62398,#62399,#62400,#62401,#62402,#62403,#62404,
#62405,#62406,#62407,#62408,#62409,#62410,#62411,#62412,#62413,#62414,#62415,
#62416,#62417,#62418,#62419,#62420,#62421,#62422,#62423,#62424,#62425,#62426,
#62427,#62428,#62429,#62430,#62431,#62432,#62433,#62434,#62435,#62436,#62437,
#62438,#62439,#62440,#62441,#62442,#62443,#62444,#62445,#62446,#62447,#62448,
#62449,#62450,#62451,#62452),.UNSPECIFIED.,.F.,.F.,(4,3,3,3,3,3,3,3,3,3,
3,3,3,3,3,3,3,3,3,3,3,3,3,3,3,3,3,3,3,3,3,3,3,3,3,3,3,3,3,3,3,3,3,3,3,3,
3,3,3,3,3,3,3,3,3,3,3,3,3,3,3,3,3,3,3,3,3,3,3,3,3,3,3,3,3,3,4),(461.814120077892,
461.910496951514,462.007387650879,462.104909978552,462.156981010936,462.240727743638,
462.324371420654,462.40793216472,462.491430026677,462.57489252724,462.658337662732,
462.741783497575,462.825248092813,462.908801278235,462.992399111808,463.07613067467,
463.155964513135,463.239711245837,463.323354922853,463.406915666919,463.490413528876,
463.573876029438,463.657321164931,463.740766999773,463.824231595011,463.907784780433,
463.991382614006,464.075114176868,464.154948015334,464.238694748036,464.322338425052,
464.405899169118,464.489397031075,464.572859531638,464.65630466713,464.739750501973,
464.823215097211,464.906768282632,464.990366116205,465.074097679067,465.153931517533,
465.237678250235,465.321321927251,465.404882671317,465.488380533274,465.571843033837,
465.655288169329,465.738734004172,465.82219859941,465.905751784832,465.989349618404,
466.073081181266,466.152915019732,466.236661752434,466.32030542945,466.403866173516,
466.487364035473,466.570826536035,466.654271671528,466.737717506371,466.821182101609,
466.90473528703,466.988333120603,467.072064683465,467.151898521931,467.234968494349,
467.317935906293,467.400821539011,467.487882019731,467.57067232615,467.653448950727,
467.736230537978,467.819035732687,467.901927051323,467.984868586552,468.06792491431,
468.097305384775),.UNSPECIFIED.);
#488=B_SPLINE_CURVE_WITH_KNOTS('',3,(#62454,#62455,#62456,#62457,#62458,
#62459,#62460,#62461,#62462,#62463,#62464,#62465,#62466,#62467,#62468,#62469,
#62470,#62471,#62472,#62473,#62474,#62475,#62476,#62477,#62478,#62479,#62480,
#62481,#62482,#62483,#62484,#62485,#62486,#62487,#62488,#62489,#62490,#62491,
#62492,#62493,#62494,#62495,#62496,#62497,#62498,#62499,#62500,#62501,#62502,
#62503,#62504,#62505,#62506,#62507,#62508,#62509,#62510,#62511,#62512,#62513,
#62514,#62515,#62516,#62517,#62518,#62519,#62520,#62521,#62522,#62523,#62524,
#62525,#62526,#62527,#62528,#62529,#62530,#62531,#62532,#62533,#62534,#62535,
#62536,#62537,#62538,#62539,#62540,#62541,#62542,#62543,#62544,#62545,#62546,
#62547,#62548,#62549,#62550,#62551,#62552,#62553,#62554,#62555,#62556,#62557,
#62558,#62559,#62560,#62561,#62562,#62563,#62564,#62565,#62566,#62567,#62568,
#62569,#62570,#62571,#62572,#62573,#62574,#62575,#62576,#62577,#62578,#62579,
#62580,#62581,#62582,#62583,#62584,#62585,#62586,#62587,#62588,#62589,#62590,
#62591,#62592,#62593,#62594,#62595,#62596,#62597,#62598,#62599,#62600,#62601,
#62602,#62603,#62604,#62605,#62606,#62607,#62608,#62609,#62610,#62611,#62612,
#62613,#62614,#62615,#62616,#62617,#62618,#62619,#62620,#62621,#62622,#62623,
#62624,#62625,#62626,#62627,#62628,#62629,#62630,#62631,#62632,#62633,#62634,
#62635,#62636,#62637,#62638,#62639,#62640,#62641,#62642,#62643,#62644,#62645,
#62646,#62647,#62648,#62649,#62650,#62651,#62652,#62653,#62654,#62655,#62656,
#62657,#62658,#62659,#62660,#62661,#62662,#62663,#62664,#62665,#62666,#62667,
#62668,#62669,#62670,#62671,#62672,#62673,#62674,#62675,#62676,#62677,#62678,
#62679,#62680,#62681,#62682),.UNSPECIFIED.,.F.,.F.,(4,3,3,3,3,3,3,3,3,3,
3,3,3,3,3,3,3,3,3,3,3,3,3,3,3,3,3,3,3,3,3,3,3,3,3,3,3,3,3,3,3,3,3,3,3,3,
3,3,3,3,3,3,3,3,3,3,3,3,3,3,3,3,3,3,3,3,3,3,3,3,3,3,3,3,3,3,4),(468.097305384879,
468.150882024131,468.234628756833,468.318272433849,468.401833177915,468.485331039872,
468.568793540435,468.652238675927,468.73568451077,468.819149106008,468.90270229143,
468.986300125003,469.070031687865,469.14986552633,469.233612259032,469.317255936048,
469.400816680114,469.484314542071,469.567777042633,469.651222178125,469.734668012968,
469.818132608206,469.901685793628,469.985283627201,470.069015190063,470.148849028529,
470.232595761231,470.316239438247,470.399800182313,470.48329804427,470.566760544833,
470.650205680325,470.733651515168,470.817116110406,470.900669295827,470.9842671294,
471.067998692262,471.147832530728,471.23157926343,471.315222940446,471.398783684512,
471.482281546469,471.565744047032,471.649189182524,471.732635017367,471.816099612605,
471.899652798026,471.983250631599,472.066982194461,472.146816032927,472.230562765629,
472.314206442645,472.397767186711,472.481265048668,472.564727549231,472.648172684723,
472.731618519566,472.815083114804,472.898636300226,472.982234133799,473.06596569666,
473.145799535126,473.229546267828,473.313189944844,473.396750688911,473.480248550867,
473.56371105143,473.647156186923,473.730602021765,473.814066617004,473.897619802425,
473.981217635998,474.06494919886,474.144783037326,474.262636864626,474.372258510993,
474.380490691925),.UNSPECIFIED.);
#489=B_SPLINE_CURVE_WITH_KNOTS('',3,(#62684,#62685,#62686,#62687,#62688,
#62689,#62690,#62691,#62692,#62693,#62694,#62695,#62696,#62697,#62698,#62699,
#62700,#62701,#62702,#62703,#62704,#62705,#62706,#62707,#62708,#62709,#62710,
#62711,#62712,#62713,#62714,#62715,#62716,#62717,#62718,#62719,#62720,#62721,
#62722,#62723,#62724,#62725,#62726,#62727,#62728,#62729,#62730,#62731,#62732,
#62733,#62734,#62735,#62736,#62737,#62738,#62739,#62740,#62741,#62742,#62743,
#62744,#62745,#62746,#62747,#62748,#62749,#62750,#62751,#62752,#62753,#62754,
#62755,#62756,#62757,#62758,#62759,#62760,#62761,#62762,#62763,#62764,#62765,
#62766,#62767,#62768,#62769,#62770,#62771,#62772,#62773,#62774,#62775,#62776,
#62777,#62778,#62779,#62780,#62781,#62782,#62783,#62784,#62785,#62786,#62787,
#62788,#62789,#62790,#62791,#62792,#62793,#62794,#62795,#62796,#62797,#62798,
#62799,#62800,#62801,#62802,#62803,#62804,#62805,#62806,#62807,#62808,#62809,
#62810,#62811,#62812,#62813,#62814,#62815,#62816,#62817,#62818,#62819,#62820,
#62821,#62822,#62823,#62824,#62825,#62826,#62827,#62828,#62829,#62830,#62831,
#62832,#62833,#62834,#62835,#62836,#62837,#62838,#62839,#62840,#62841,#62842,
#62843,#62844,#62845,#62846,#62847,#62848,#62849,#62850,#62851,#62852,#62853,
#62854,#62855,#62856,#62857,#62858,#62859,#62860,#62861,#62862,#62863,#62864,
#62865,#62866,#62867,#62868,#62869,#62870,#62871,#62872,#62873,#62874,#62875,
#62876,#62877,#62878,#62879,#62880,#62881,#62882,#62883,#62884,#62885,#62886,
#62887,#62888,#62889,#62890,#62891,#62892,#62893,#62894,#62895,#62896,#62897,
#62898,#62899,#62900,#62901,#62902,#62903,#62904,#62905,#62906,#62907,#62908,
#62909,#62910,#62911,#62912),.UNSPECIFIED.,.F.,.F.,(4,3,3,3,3,3,3,3,3,3,
3,3,3,3,3,3,3,3,3,3,3,3,3,3,3,3,3,3,3,3,3,3,3,3,3,3,3,3,3,3,3,3,3,3,3,3,
3,3,3,3,3,3,3,3,3,3,3,3,3,3,3,3,3,3,3,3,3,3,3,3,3,3,3,3,3,3,4),(474.380490692059,
474.462988466164,474.548085725334,474.630497101718,474.71289802157,474.795307390673,
474.877744118907,474.96027069151,475.042851238611,475.12554651215,475.143766539525,
475.227513272227,475.311156949243,475.394717693309,475.478215555266,475.561678055828,
475.645123191321,475.728569026163,475.812033621402,475.895586806824,475.979184640396,
476.062916203258,476.142750041724,476.226496774426,476.310140451442,476.393701195508,
476.477199057465,476.560661558028,476.64410669352,476.727552528363,476.811017123601,
476.894570309023,476.978168142596,477.061899705458,477.141733543923,477.225480276625,
477.309123953641,477.392684697707,477.476182559663,477.559645060226,477.643090195718,
477.726536030561,477.810000625799,477.893553811221,477.977151644793,478.060883207655,
478.140717046122,478.224463778824,478.30810745584,478.391668199906,478.475166061863,
478.558628562425,478.642073697918,478.725519532761,478.808984127999,478.892537313421,
478.976135146994,479.059866709856,479.139700548321,479.223447281023,479.307090958039,
479.390651702105,479.474149564062,479.557612064625,479.641057200117,479.72450303496,
479.807967630198,479.89152081562,479.975118649192,480.058850212054,480.138684050521,
480.225798891272,480.31277593033,480.400500947557,480.487201398599,480.575438698919,
480.663675999239),.UNSPECIFIED.);
#490=B_SPLINE_CURVE_WITH_KNOTS('',3,(#62914,#62915,#62916,#62917,#62918,
#62919,#62920,#62921,#62922,#62923,#62924,#62925,#62926,#62927,#62928,#62929,
#62930,#62931,#62932,#62933,#62934,#62935,#62936,#62937,#62938,#62939,#62940,
#62941,#62942,#62943,#62944,#62945,#62946,#62947,#62948,#62949,#62950,#62951,
#62952,#62953,#62954,#62955,#62956,#62957,#62958,#62959,#62960,#62961,#62962,
#62963,#62964,#62965,#62966,#62967,#62968,#62969,#62970,#62971,#62972,#62973,
#62974,#62975,#62976,#62977,#62978,#62979,#62980,#62981,#62982,#62983,#62984,
#62985,#62986,#62987,#62988,#62989,#62990,#62991,#62992,#62993,#62994,#62995,
#62996,#62997,#62998,#62999,#63000,#63001,#63002,#63003,#63004,#63005,#63006,
#63007,#63008,#63009,#63010,#63011,#63012,#63013,#63014,#63015,#63016,#63017,
#63018,#63019,#63020,#63021,#63022,#63023,#63024,#63025,#63026,#63027,#63028,
#63029,#63030,#63031,#63032,#63033,#63034,#63035,#63036,#63037,#63038,#63039,
#63040,#63041,#63042,#63043,#63044,#63045,#63046,#63047,#63048,#63049,#63050,
#63051,#63052,#63053,#63054,#63055,#63056,#63057,#63058,#63059,#63060,#63061,
#63062,#63063,#63064,#63065,#63066,#63067,#63068,#63069,#63070,#63071,#63072,
#63073,#63074,#63075,#63076,#63077,#63078,#63079,#63080,#63081,#63082,#63083,
#63084,#63085,#63086,#63087,#63088,#63089,#63090,#63091,#63092,#63093,#63094,
#63095,#63096,#63097,#63098,#63099,#63100,#63101,#63102,#63103,#63104,#63105,
#63106,#63107,#63108,#63109,#63110,#63111,#63112,#63113,#63114,#63115,#63116,
#63117,#63118,#63119,#63120,#63121,#63122,#63123,#63124,#63125,#63126,#63127,
#63128,#63129,#63130,#63131,#63132,#63133,#63134,#63135,#63136,#63137,#63138,
#63139,#63140,#63141,#63142),.UNSPECIFIED.,.F.,.F.,(4,3,3,3,3,3,3,3,3,3,
3,3,3,3,3,3,3,3,3,3,3,3,3,3,3,3,3,3,3,3,3,3,3,3,3,3,3,3,3,3,3,3,3,3,3,3,
3,3,3,3,3,3,3,3,3,3,3,3,3,3,3,3,3,3,3,3,3,3,3,3,3,3,3,3,3,3,4),(480.663675999356,
480.752067585733,480.840612156768,480.929400150455,481.018321197254,481.10745040222,
481.13766755272,481.221414285422,481.305057962438,481.388618706504,481.472116568461,
481.555579069024,481.639024204516,481.722470039359,481.805934634597,481.889487820019,
481.973085653591,482.056817216453,482.136651054919,482.220397787621,482.304041464637,
482.387602208703,482.47110007066,482.554562571223,482.638007706715,482.721453541558,
482.804918136796,482.888471322218,482.972069155791,483.055800718653,483.135634557118,
483.21938128982,483.303024966836,483.386585710902,483.470083572859,483.553546073421,
483.636991208913,483.720437043756,483.803901638994,483.887454824416,483.971052657989,
484.05478422085,484.134618059317,484.218364792019,484.302008469035,484.385569213101,
484.469067075058,484.552529575621,484.635974711113,484.719420545956,484.802885141194,
484.886438326616,484.970036160189,485.053767723051,485.133601561516,485.217348294218,
485.300991971234,485.3845527153,485.468050577257,485.551513077819,485.634958213312,
485.718404048154,485.801868643393,485.885421828814,485.969019662387,486.052751225249,
486.132585063716,486.215094552444,486.297501225616,486.379814785946,486.462076176782,
486.544304464461,486.626518684454,486.708772128317,486.791043622075,486.873405145217,
486.946861306276),.UNSPECIFIED.);
#491=B_SPLINE_CURVE_WITH_KNOTS('',3,(#63144,#63145,#63146,#63147,#63148,
#63149,#63150,#63151,#63152,#63153,#63154,#63155,#63156,#63157,#63158,#63159,
#63160,#63161,#63162,#63163,#63164,#63165,#63166,#63167,#63168,#63169,#63170,
#63171,#63172,#63173,#63174,#63175,#63176,#63177,#63178,#63179,#63180,#63181,
#63182,#63183,#63184,#63185,#63186,#63187,#63188,#63189,#63190,#63191,#63192,
#63193,#63194,#63195,#63196,#63197,#63198,#63199,#63200,#63201,#63202,#63203,
#63204,#63205,#63206,#63207,#63208,#63209,#63210,#63211,#63212,#63213,#63214,
#63215,#63216,#63217,#63218,#63219,#63220,#63221,#63222,#63223,#63224,#63225,
#63226,#63227,#63228,#63229,#63230,#63231,#63232,#63233,#63234,#63235,#63236,
#63237,#63238,#63239,#63240,#63241,#63242,#63243,#63244,#63245,#63246,#63247,
#63248,#63249,#63250,#63251,#63252,#63253,#63254,#63255,#63256,#63257,#63258,
#63259,#63260,#63261,#63262,#63263,#63264,#63265,#63266,#63267,#63268,#63269,
#63270,#63271,#63272,#63273,#63274,#63275,#63276,#63277,#63278,#63279,#63280,
#63281,#63282,#63283,#63284,#63285,#63286,#63287,#63288,#63289,#63290,#63291,
#63292,#63293,#63294,#63295,#63296,#63297,#63298,#63299,#63300,#63301,#63302,
#63303,#63304,#63305,#63306,#63307,#63308,#63309,#63310,#63311,#63312,#63313,
#63314,#63315,#63316,#63317,#63318,#63319,#63320,#63321,#63322,#63323,#63324,
#63325,#63326,#63327,#63328,#63329,#63330,#63331,#63332,#63333,#63334,#63335,
#63336,#63337,#63338,#63339,#63340,#63341,#63342,#63343,#63344,#63345,#63346,
#63347,#63348,#63349,#63350,#63351,#63352,#63353,#63354,#63355,#63356,#63357,
#63358,#63359,#63360,#63361,#63362,#63363,#63364,#63365,#63366,#63367,#63368,
#63369),.UNSPECIFIED.,.F.,.F.,(4,3,3,3,3,3,3,3,3,3,3,3,3,3,3,3,3,3,3,3,
3,3,3,3,3,3,3,3,3,3,3,3,3,3,3,3,3,3,3,3,3,3,3,3,3,3,3,3,3,3,3,3,3,3,3,3,
3,3,3,3,3,3,3,3,3,3,3,3,3,3,3,3,3,3,3,4),(486.946861306418,487.07206518107,
487.131568565915,487.215315298617,487.298958975633,487.382519719699,487.466017581656,
487.549480082219,487.632925217711,487.716371052554,487.799835647792,487.883388833214,
487.966986666787,488.050718229649,488.130552068114,488.214298800816,488.297942477832,
488.381503221898,488.465001083855,488.548463584417,488.63190871991,488.715354554752,
488.79881914999,488.882372335412,488.965970168985,489.049701731847,489.129535570313,
489.213282303015,489.296925980031,489.380486724097,489.463984586054,489.547447086617,
489.630892222109,489.714338056952,489.79780265219,489.881355837612,489.964953671184,
490.048685234046,490.128519072512,490.212265805214,490.29590948223,490.379470226296,
490.462968088253,490.546430588816,490.629875724308,490.713321559151,490.796786154389,
490.880339339811,490.963937173383,491.047668736245,491.127502574711,491.211249307413,
491.294892984429,491.378453728495,491.461951590452,491.545414091015,491.628859226507,
491.71230506135,491.795769656588,491.87932284201,491.962920675583,492.046652238445,
492.126486076911,492.210232809613,492.293876486629,492.377437230695,492.460935092652,
492.544397593215,492.627842728707,492.71128856355,492.794753158788,492.87830634421,
492.961904177783,493.045635740645,493.12546957911,493.230046613598),
 .UNSPECIFIED.);
#492=B_SPLINE_CURVE_WITH_KNOTS('',3,(#63371,#63372,#63373,#63374,#63375,
#63376,#63377,#63378,#63379,#63380,#63381,#63382,#63383,#63384,#63385,#63386,
#63387,#63388,#63389,#63390,#63391,#63392,#63393,#63394,#63395,#63396,#63397,
#63398,#63399,#63400,#63401,#63402,#63403,#63404,#63405,#63406,#63407,#63408,
#63409,#63410,#63411,#63412,#63413,#63414,#63415,#63416,#63417,#63418,#63419,
#63420,#63421,#63422,#63423,#63424,#63425,#63426,#63427,#63428,#63429,#63430,
#63431,#63432,#63433,#63434,#63435,#63436,#63437,#63438,#63439,#63440,#63441,
#63442,#63443,#63444,#63445,#63446,#63447,#63448,#63449,#63450,#63451,#63452,
#63453,#63454,#63455,#63456,#63457,#63458,#63459,#63460,#63461,#63462,#63463,
#63464,#63465,#63466,#63467,#63468,#63469,#63470,#63471,#63472,#63473,#63474,
#63475,#63476,#63477,#63478,#63479,#63480,#63481,#63482,#63483,#63484,#63485,
#63486,#63487,#63488,#63489,#63490,#63491,#63492,#63493,#63494,#63495,#63496,
#63497,#63498,#63499,#63500,#63501,#63502,#63503,#63504,#63505,#63506,#63507,
#63508,#63509,#63510,#63511,#63512,#63513,#63514,#63515,#63516,#63517,#63518,
#63519,#63520,#63521,#63522,#63523,#63524,#63525,#63526,#63527,#63528,#63529,
#63530,#63531,#63532,#63533,#63534,#63535,#63536,#63537,#63538,#63539,#63540,
#63541,#63542,#63543,#63544,#63545,#63546,#63547,#63548,#63549,#63550,#63551,
#63552,#63553,#63554,#63555,#63556,#63557,#63558,#63559,#63560,#63561,#63562,
#63563,#63564,#63565,#63566,#63567,#63568,#63569,#63570,#63571,#63572,#63573,
#63574,#63575,#63576,#63577,#63578,#63579,#63580,#63581,#63582,#63583,#63584,
#63585,#63586,#63587,#63588,#63589,#63590,#63591,#63592,#63593,#63594,#63595,
#63596,#63597,#63598,#63599),.UNSPECIFIED.,.F.,.F.,(4,3,3,3,3,3,3,3,3,3,
3,3,3,3,3,3,3,3,3,3,3,3,3,3,3,3,3,3,3,3,3,3,3,3,3,3,3,3,3,3,3,3,3,3,3,3,
3,3,3,3,3,3,3,3,3,3,3,3,3,3,3,3,3,3,3,3,3,3,3,3,3,3,3,3,3,3,4),(493.230046613733,
493.312666057369,493.39519384848,493.477651040569,493.560063491413,493.642453340751,
493.7248395128,493.807240926367,493.889725936625,493.972254060176,494.054910316146,
494.124453081309,494.208199814011,494.291843491027,494.375404235093,494.45890209705,
494.542364597612,494.625809733104,494.709255567947,494.792720163185,494.876273348607,
494.95987118218,495.043602745042,495.123436583508,495.20718331621,495.290826993226,
495.374387737292,495.457885599249,495.541348099812,495.624793235304,495.708239070147,
495.791703665384,495.875256850806,495.958854684379,496.042586247241,496.122420085707,
496.206166818409,496.289810495425,496.373371239491,496.456869101448,496.540331602011,
496.623776737503,496.707222572346,496.790687167584,496.874240353006,496.957838186578,
497.04156974944,497.121403587906,497.205150320608,497.288793997624,497.37235474169,
497.455852603647,497.53931510421,497.622760239702,497.706206074545,497.789670669783,
497.873223855205,497.956821688778,498.04055325164,498.120387090106,498.204133822808,
498.287777499824,498.371338243891,498.454836105847,498.53829860641,498.621743741902,
498.705189576745,498.788654171983,498.872207357405,498.955805190978,499.03953675384,
499.119370592305,499.217835924377,499.311002515681,499.403889327138,499.496350686817,
499.513231920595),.UNSPECIFIED.);
#493=B_SPLINE_CURVE_WITH_KNOTS('',3,(#63601,#63602,#63603,#63604,#63605,
#63606,#63607,#63608,#63609,#63610,#63611,#63612,#63613,#63614,#63615,#63616,
#63617,#63618,#63619,#63620,#63621,#63622,#63623,#63624,#63625,#63626,#63627,
#63628,#63629,#63630,#63631,#63632,#63633,#63634,#63635,#63636,#63637,#63638,
#63639,#63640,#63641,#63642,#63643,#63644,#63645,#63646,#63647,#63648,#63649,
#63650,#63651,#63652,#63653,#63654,#63655,#63656,#63657,#63658,#63659,#63660,
#63661,#63662,#63663,#63664,#63665,#63666,#63667,#63668,#63669,#63670,#63671,
#63672,#63673,#63674,#63675,#63676,#63677,#63678,#63679,#63680,#63681,#63682,
#63683,#63684,#63685,#63686,#63687,#63688,#63689,#63690,#63691,#63692,#63693,
#63694,#63695,#63696,#63697,#63698,#63699,#63700,#63701,#63702,#63703,#63704,
#63705,#63706,#63707,#63708,#63709,#63710,#63711,#63712,#63713,#63714,#63715,
#63716,#63717,#63718,#63719,#63720,#63721,#63722,#63723,#63724,#63725,#63726,
#63727,#63728,#63729,#63730,#63731,#63732,#63733,#63734,#63735,#63736,#63737,
#63738,#63739,#63740,#63741,#63742,#63743,#63744,#63745,#63746,#63747,#63748,
#63749,#63750,#63751,#63752,#63753,#63754,#63755,#63756,#63757,#63758,#63759,
#63760,#63761,#63762,#63763,#63764,#63765,#63766,#63767,#63768,#63769,#63770,
#63771,#63772,#63773,#63774,#63775,#63776,#63777,#63778,#63779,#63780,#63781,
#63782,#63783,#63784,#63785,#63786,#63787,#63788,#63789,#63790,#63791,#63792,
#63793,#63794,#63795,#63796,#63797,#63798,#63799,#63800,#63801,#63802,#63803,
#63804,#63805,#63806,#63807,#63808,#63809,#63810,#63811,#63812,#63813,#63814,
#63815,#63816,#63817,#63818,#63819,#63820,#63821,#63822,#63823,#63824,#63825,
#63826,#63827,#63828,#63829,#63830,#63831,#63832),.UNSPECIFIED.,.F.,.F.,
(4,3,3,3,3,3,3,3,3,3,3,3,3,3,3,3,3,3,3,3,3,3,3,3,3,3,3,3,3,3,3,3,3,3,3,
3,3,3,3,3,3,3,3,3,3,3,3,3,3,3,3,3,3,3,3,3,3,3,3,3,3,3,3,3,3,3,3,3,3,3,3,
3,3,3,3,3,3,4),(499.513231920777,499.597681186419,499.682149034449,499.766652032328,
499.854577547872,499.939253202636,500.024000450852,500.10887777593,500.118354094504,
500.202100827206,500.285744504222,500.369305248288,500.452803110245,500.536265610808,
500.6197107463,500.703156581143,500.786621176381,500.870174361803,500.953772195375,
501.037503758237,501.117337596703,501.201084329405,501.284728006421,501.368288750487,
501.451786612444,501.535249113007,501.618694248499,501.702140083341,501.78560467858,
501.869157864001,501.952755697574,502.036487260436,502.116321098902,502.200067831604,
502.28371150862,502.367272252687,502.450770114643,502.534232615206,502.617677750698,
502.701123585541,502.784588180779,502.8681413662,502.951739199773,503.035470762635,
503.115304601101,503.199051333803,503.282695010819,503.366255754885,503.449753616842,
503.533216117404,503.616661252897,503.70010708774,503.783571682978,503.8671248684,
503.950722701972,504.034454264834,504.114288103301,504.198034836003,504.281678513019,
504.365239257085,504.448737119042,504.532199619605,504.615644755097,504.69909058994,
504.782555185178,504.8661083706,504.949706204172,505.033437767034,505.1132716055,
505.198664808307,505.282006113707,505.365267837759,505.448468382632,505.535455593963,
505.618597993435,505.701733921829,505.784896160721,505.796417227957),
 .UNSPECIFIED.);
#494=B_SPLINE_CURVE_WITH_KNOTS('',3,(#63834,#63835,#63836,#63837,#63838,
#63839,#63840,#63841,#63842,#63843,#63844,#63845,#63846,#63847,#63848,#63849,
#63850,#63851,#63852,#63853,#63854,#63855,#63856,#63857,#63858,#63859,#63860,
#63861,#63862,#63863,#63864,#63865,#63866,#63867,#63868,#63869,#63870,#63871,
#63872,#63873,#63874,#63875,#63876,#63877,#63878,#63879,#63880,#63881,#63882,
#63883,#63884,#63885,#63886,#63887,#63888,#63889,#63890,#63891,#63892,#63893,
#63894,#63895,#63896,#63897,#63898,#63899,#63900,#63901,#63902,#63903,#63904,
#63905,#63906,#63907,#63908,#63909,#63910,#63911,#63912,#63913,#63914,#63915,
#63916,#63917,#63918,#63919,#63920,#63921,#63922,#63923,#63924,#63925,#63926,
#63927,#63928,#63929,#63930,#63931,#63932,#63933,#63934,#63935,#63936,#63937,
#63938,#63939,#63940,#63941,#63942,#63943,#63944,#63945,#63946,#63947,#63948,
#63949,#63950,#63951,#63952,#63953,#63954,#63955,#63956,#63957,#63958,#63959,
#63960,#63961,#63962,#63963,#63964,#63965,#63966,#63967,#63968,#63969,#63970,
#63971,#63972,#63973,#63974,#63975,#63976,#63977,#63978,#63979,#63980,#63981,
#63982,#63983,#63984,#63985,#63986,#63987,#63988,#63989,#63990,#63991,#63992,
#63993,#63994,#63995,#63996,#63997,#63998,#63999,#64000,#64001,#64002,#64003,
#64004,#64005,#64006,#64007,#64008,#64009,#64010,#64011,#64012,#64013,#64014,
#64015,#64016,#64017,#64018,#64019,#64020,#64021,#64022,#64023,#64024,#64025,
#64026,#64027,#64028,#64029,#64030,#64031,#64032,#64033,#64034,#64035,#64036,
#64037,#64038,#64039,#64040,#64041,#64042,#64043,#64044,#64045,#64046,#64047,
#64048,#64049,#64050,#64051,#64052,#64053,#64054,#64055,#64056,#64057,#64058,
#64059,#64060,#64061,#64062),.UNSPECIFIED.,.F.,.F.,(4,3,3,3,3,3,3,3,3,3,
3,3,3,3,3,3,3,3,3,3,3,3,3,3,3,3,3,3,3,3,3,3,3,3,3,3,3,3,3,3,3,3,3,3,3,3,
3,3,3,3,3,3,3,3,3,3,3,3,3,3,3,3,3,3,3,3,3,3,3,3,3,3,3,3,3,3,4),(505.796417228126,
505.895263971297,505.994821585573,506.095146411306,506.112255107699,506.196001840401,
506.279645517416,506.363206261483,506.446704123439,506.530166624002,506.613611759494,
506.697057594336,506.780522189574,506.864075374996,506.947673208569,507.03140477143,
507.111238609898,507.1949853426,507.278629019616,507.362189763682,507.445687625639,
507.529150126201,507.612595261694,507.696041096536,507.779505691775,507.863058877196,
507.946656710769,508.030388273631,508.110222112097,508.193968844799,508.277612521815,
508.361173265881,508.444671127838,508.528133628401,508.611578763893,508.695024598736,
508.778489193974,508.862042379396,508.945640212969,509.029371775831,509.109205614296,
509.192952346998,509.276596024014,509.36015676808,509.443654630037,509.527117130599,
509.610562266092,509.694008100934,509.777472696172,509.861025881594,509.944623715167,
510.028355278029,510.108189116495,510.191935849197,510.275579526213,510.359140270279,
510.442638132236,510.526100632799,510.609545768291,510.692991603134,510.776456198372,
510.860009383794,510.943607217366,511.027338780228,511.107172618695,511.190549520313,
511.273823599296,511.357015357863,511.440145222664,511.523241197348,511.606321370413,
511.689404142631,511.772507912952,511.8556995516,511.938938518477,512.022303089775,
512.079602535017),.UNSPECIFIED.);
#495=B_SPLINE_CURVE_WITH_KNOTS('',3,(#64064,#64065,#64066,#64067,#64068,
#64069,#64070,#64071,#64072,#64073,#64074,#64075,#64076,#64077,#64078,#64079,
#64080,#64081,#64082,#64083,#64084,#64085,#64086,#64087,#64088,#64089,#64090,
#64091,#64092,#64093,#64094,#64095,#64096,#64097,#64098,#64099,#64100,#64101,
#64102,#64103,#64104,#64105,#64106,#64107,#64108,#64109,#64110,#64111,#64112,
#64113,#64114,#64115,#64116,#64117,#64118,#64119,#64120,#64121,#64122,#64123,
#64124,#64125,#64126,#64127,#64128,#64129,#64130,#64131,#64132,#64133,#64134,
#64135,#64136,#64137,#64138,#64139,#64140,#64141,#64142,#64143,#64144,#64145,
#64146,#64147,#64148,#64149,#64150,#64151,#64152,#64153,#64154,#64155,#64156,
#64157,#64158,#64159,#64160,#64161,#64162,#64163,#64164,#64165,#64166,#64167,
#64168,#64169,#64170,#64171,#64172,#64173,#64174,#64175,#64176,#64177,#64178,
#64179,#64180,#64181,#64182,#64183,#64184,#64185,#64186,#64187,#64188,#64189,
#64190,#64191,#64192,#64193,#64194,#64195,#64196,#64197,#64198,#64199,#64200,
#64201,#64202,#64203,#64204,#64205,#64206,#64207,#64208,#64209,#64210,#64211,
#64212,#64213,#64214,#64215,#64216,#64217,#64218,#64219,#64220,#64221,#64222,
#64223,#64224,#64225,#64226,#64227,#64228,#64229,#64230,#64231,#64232,#64233,
#64234,#64235,#64236,#64237,#64238,#64239,#64240,#64241,#64242,#64243,#64244,
#64245,#64246,#64247,#64248,#64249,#64250,#64251,#64252,#64253,#64254,#64255,
#64256,#64257,#64258,#64259,#64260,#64261,#64262,#64263,#64264,#64265,#64266,
#64267,#64268,#64269,#64270,#64271,#64272,#64273,#64274,#64275,#64276,#64277,
#64278,#64279,#64280,#64281,#64282,#64283,#64284,#64285,#64286,#64287,#64288,
#64289,#64290,#64291,#64292),.UNSPECIFIED.,.F.,.F.,(4,3,3,3,3,3,3,3,3,3,
3,3,3,3,3,3,3,3,3,3,3,3,3,3,3,3,3,3,3,3,3,3,3,3,3,3,3,3,3,3,3,3,3,3,3,3,
3,3,3,3,3,3,3,3,3,3,3,3,3,3,3,3,3,3,3,3,3,3,3,3,3,3,3,3,3,3,4),(512.079602535136,
512.106156120894,512.189902853596,512.273546530612,512.357107274678,512.440605136635,
512.524067637198,512.60751277269,512.690958607533,512.774423202771,512.857976388193,
512.941574221766,513.025305784627,513.105139623093,513.188886355795,513.272530032811,
513.356090776877,513.439588638834,513.523051139396,513.606496274889,513.689942109731,
513.773406704969,513.856959890391,513.940557723964,514.024289286826,514.104123125292,
514.187869857994,514.27151353501,514.355074279076,514.438572141033,514.522034641596,
514.605479777088,514.688925611931,514.772390207169,514.855943392591,514.939541226164,
515.023272789026,515.103106627491,515.186853360193,515.270497037209,515.354057781275,
515.437555643232,515.521018143795,515.604463279287,515.68790911413,515.771373709368,
515.85492689479,515.938524728363,516.022256291224,516.102090129691,516.185836862393,
516.269480539409,516.353041283475,516.436539145432,516.520001645995,516.603446781487,
516.68689261633,516.770357211568,516.85391039699,516.937508230563,517.021239793425,
517.10107363189,517.184820364592,517.268464041608,517.352024785674,517.435522647631,
517.518985148193,517.602430283686,517.685876118528,517.769340713767,517.852893899189,
517.936491732761,518.020223295623,518.100057134089,518.207488261823,518.312945017838,
518.362787842169),.UNSPECIFIED.);
#496=B_SPLINE_CURVE_WITH_KNOTS('',3,(#64294,#64295,#64296,#64297,#64298,
#64299,#64300,#64301,#64302,#64303,#64304,#64305,#64306,#64307,#64308,#64309,
#64310,#64311,#64312,#64313,#64314,#64315,#64316,#64317,#64318,#64319,#64320,
#64321,#64322,#64323,#64324,#64325,#64326,#64327,#64328,#64329,#64330,#64331,
#64332,#64333,#64334,#64335,#64336,#64337,#64338,#64339,#64340,#64341,#64342,
#64343,#64344,#64345,#64346,#64347,#64348,#64349,#64350,#64351,#64352,#64353,
#64354,#64355,#64356,#64357,#64358,#64359,#64360,#64361,#64362,#64363,#64364,
#64365,#64366,#64367,#64368,#64369,#64370,#64371,#64372,#64373,#64374,#64375,
#64376,#64377,#64378,#64379,#64380,#64381,#64382,#64383,#64384,#64385,#64386,
#64387,#64388,#64389,#64390,#64391,#64392,#64393,#64394,#64395,#64396,#64397,
#64398,#64399,#64400,#64401,#64402,#64403,#64404,#64405,#64406,#64407,#64408,
#64409,#64410,#64411,#64412,#64413,#64414,#64415,#64416,#64417,#64418,#64419,
#64420,#64421,#64422,#64423,#64424,#64425,#64426,#64427,#64428,#64429,#64430,
#64431,#64432,#64433,#64434,#64435,#64436,#64437,#64438,#64439,#64440,#64441,
#64442,#64443,#64444,#64445,#64446,#64447,#64448,#64449,#64450,#64451,#64452,
#64453,#64454,#64455,#64456,#64457,#64458,#64459,#64460,#64461,#64462,#64463,
#64464,#64465,#64466,#64467,#64468,#64469,#64470,#64471,#64472,#64473,#64474,
#64475,#64476,#64477,#64478,#64479,#64480,#64481,#64482,#64483,#64484,#64485,
#64486,#64487,#64488,#64489,#64490,#64491,#64492,#64493,#64494,#64495,#64496,
#64497,#64498,#64499,#64500,#64501,#64502,#64503,#64504,#64505,#64506,#64507,
#64508,#64509,#64510,#64511,#64512,#64513,#64514,#64515,#64516,#64517,#64518,
#64519,#64520,#64521,#64522),.UNSPECIFIED.,.F.,.F.,(4,3,3,3,3,3,3,3,3,3,
3,3,3,3,3,3,3,3,3,3,3,3,3,3,3,3,3,3,3,3,3,3,3,3,3,3,3,3,3,3,3,3,3,3,3,3,
3,3,3,3,3,3,3,3,3,3,3,3,3,3,3,3,3,3,3,3,3,3,3,3,3,3,3,3,3,3,4),(518.362787842316,
518.44544362937,518.528056518539,518.61064778964,518.693236220728,518.775840584852,
518.85853037429,518.941263594348,519.024128204109,519.099040636288,519.18278736899,
519.266431046006,519.349991790072,519.433489652029,519.516952152591,519.600397288083,
519.683843122926,519.767307718164,519.850860903586,519.934458737158,520.01819030002,
520.098024138487,520.181770871189,520.265414548205,520.348975292271,520.432473154228,
520.515935654791,520.599380790283,520.682826625126,520.766291220364,520.849844405786,
520.933442239359,521.01717380222,521.097007640686,521.180754373388,521.264398050404,
521.34795879447,521.431456656427,521.51491915699,521.598364292482,521.681810127325,
521.765274722563,521.848827907985,521.932425741557,522.016157304419,522.095991142886,
522.179737875588,522.263381552604,522.346942296671,522.430440158627,522.51390265919,
522.597347794682,522.680793629525,522.764258224764,522.847811410185,522.931409243758,
523.01514080662,523.094974645085,523.178721377787,523.262365054803,523.345925798869,
523.429423660825,523.512886161388,523.596331296881,523.679777131724,523.763241726962,
523.846794912384,523.930392745956,524.014124308818,524.093958147284,524.180198977607,
524.266313373394,524.352315450507,524.438191058093,524.523991974352,524.609717033682,
524.645973149496),.UNSPECIFIED.);
#497=B_SPLINE_CURVE_WITH_KNOTS('',3,(#64524,#64525,#64526,#64527,#64528,
#64529,#64530,#64531,#64532,#64533,#64534,#64535,#64536,#64537,#64538,#64539,
#64540,#64541,#64542,#64543,#64544,#64545,#64546,#64547,#64548,#64549,#64550,
#64551,#64552,#64553,#64554,#64555,#64556,#64557,#64558,#64559,#64560,#64561,
#64562,#64563,#64564,#64565,#64566,#64567,#64568,#64569,#64570,#64571,#64572,
#64573,#64574,#64575,#64576,#64577,#64578,#64579,#64580,#64581,#64582,#64583,
#64584,#64585,#64586,#64587,#64588,#64589,#64590,#64591,#64592,#64593,#64594,
#64595,#64596,#64597,#64598,#64599,#64600,#64601,#64602,#64603,#64604,#64605,
#64606,#64607,#64608,#64609,#64610,#64611,#64612,#64613,#64614,#64615,#64616,
#64617,#64618,#64619,#64620,#64621,#64622,#64623,#64624,#64625,#64626,#64627,
#64628,#64629,#64630,#64631,#64632,#64633,#64634,#64635,#64636,#64637,#64638,
#64639,#64640,#64641,#64642,#64643,#64644,#64645,#64646,#64647,#64648,#64649,
#64650,#64651,#64652,#64653,#64654,#64655,#64656,#64657,#64658,#64659,#64660,
#64661,#64662,#64663,#64664,#64665,#64666,#64667,#64668,#64669,#64670,#64671,
#64672,#64673,#64674,#64675,#64676,#64677,#64678,#64679,#64680,#64681,#64682,
#64683,#64684,#64685,#64686,#64687,#64688,#64689,#64690,#64691,#64692,#64693,
#64694,#64695,#64696,#64697,#64698,#64699,#64700,#64701,#64702,#64703,#64704,
#64705,#64706,#64707,#64708,#64709,#64710,#64711,#64712,#64713,#64714,#64715,
#64716,#64717,#64718,#64719,#64720,#64721,#64722,#64723,#64724,#64725,#64726,
#64727,#64728,#64729,#64730,#64731,#64732,#64733,#64734,#64735,#64736,#64737,
#64738,#64739,#64740,#64741,#64742,#64743,#64744,#64745,#64746,#64747,#64748,
#64749,#64750,#64751,#64752),.UNSPECIFIED.,.F.,.F.,(4,3,3,3,3,3,3,3,3,3,
3,3,3,3,3,3,3,3,3,3,3,3,3,3,3,3,3,3,3,3,3,3,3,3,3,3,3,3,3,3,3,3,3,3,3,3,
3,3,3,3,3,3,3,3,3,3,3,3,3,3,3,3,3,3,3,3,3,3,3,3,3,3,3,3,3,3,4),(524.645973149609,
524.735551576018,524.825461875191,524.915537276957,525.005896438371,525.092941649483,
525.176688382185,525.260332059201,525.343892803268,525.427390665224,525.510853165787,
525.594298301279,525.677744136122,525.76120873136,525.844761916782,525.928359750355,
526.012091313217,526.091925151682,526.175671884384,526.2593155614,526.342876305466,
526.426374167423,526.509836667985,526.593281803477,526.67672763832,526.760192233558,
526.84374541898,526.927343252553,527.011074815414,527.090908653881,527.174655386583,
527.258299063599,527.341859807665,527.425357669622,527.508820170185,527.592265305677,
527.67571114052,527.759175735758,527.84272892118,527.926326754752,528.010058317614,
528.08989215608,528.173638888782,528.257282565798,528.340843309865,528.424341171821,
528.507803672384,528.591248807876,528.674694642719,528.758159237957,528.841712423379,
528.925310256952,529.009041819814,529.08887565828,529.172622390982,529.256266067998,
529.339826812064,529.423324674021,529.506787174584,529.590232310076,529.673678144919,
529.757142740157,529.840695925579,529.924293759152,530.008025322014,530.087859160479,
530.170361360948,530.252761152824,530.337310815793,530.41956603867,530.50178925204,
530.583999493628,530.670289234364,530.752565445803,530.834878351078,530.917278863106,
530.929158456571),.UNSPECIFIED.);
#498=B_SPLINE_CURVE_WITH_KNOTS('',3,(#64754,#64755,#64756,#64757,#64758,
#64759,#64760,#64761,#64762,#64763,#64764,#64765,#64766,#64767,#64768,#64769,
#64770,#64771,#64772,#64773,#64774,#64775,#64776,#64777,#64778,#64779,#64780,
#64781,#64782,#64783,#64784,#64785,#64786,#64787,#64788,#64789,#64790,#64791,
#64792,#64793,#64794,#64795,#64796,#64797,#64798,#64799,#64800,#64801,#64802,
#64803,#64804,#64805,#64806,#64807,#64808,#64809,#64810,#64811,#64812,#64813,
#64814,#64815,#64816,#64817,#64818,#64819,#64820,#64821,#64822,#64823,#64824,
#64825,#64826,#64827,#64828,#64829,#64830,#64831,#64832,#64833,#64834,#64835,
#64836,#64837,#64838,#64839,#64840,#64841,#64842,#64843,#64844,#64845,#64846,
#64847,#64848,#64849,#64850,#64851,#64852,#64853,#64854,#64855,#64856,#64857,
#64858,#64859,#64860,#64861,#64862,#64863,#64864,#64865,#64866,#64867,#64868,
#64869,#64870,#64871,#64872,#64873,#64874,#64875,#64876,#64877,#64878,#64879,
#64880,#64881,#64882,#64883,#64884,#64885,#64886,#64887,#64888,#64889,#64890,
#64891,#64892,#64893,#64894,#64895,#64896,#64897,#64898,#64899,#64900,#64901,
#64902,#64903,#64904,#64905,#64906,#64907,#64908,#64909,#64910,#64911,#64912,
#64913,#64914,#64915,#64916,#64917,#64918,#64919,#64920,#64921,#64922,#64923,
#64924,#64925,#64926,#64927,#64928,#64929,#64930,#64931,#64932,#64933,#64934,
#64935,#64936,#64937,#64938,#64939,#64940,#64941,#64942,#64943,#64944,#64945,
#64946,#64947,#64948,#64949,#64950,#64951,#64952,#64953,#64954,#64955,#64956,
#64957,#64958,#64959,#64960,#64961,#64962,#64963,#64964,#64965,#64966,#64967,
#64968,#64969,#64970,#64971,#64972,#64973,#64974,#64975,#64976,#64977,#64978,
#64979),.UNSPECIFIED.,.F.,.F.,(4,3,3,3,3,3,3,3,3,3,3,3,3,3,3,3,3,3,3,3,
3,3,3,3,3,3,3,3,3,3,3,3,3,3,3,3,3,3,3,3,3,3,3,3,3,3,3,3,3,3,3,3,3,3,3,3,
3,3,3,3,3,3,3,3,3,3,3,3,3,3,3,3,3,3,3,4),(530.929158456675,531.066685078122,
531.086842662678,531.17058939538,531.254233072396,531.337793816463,531.42129167842,
531.504754178982,531.588199314475,531.671645149318,531.755109744556,531.838662929978,
531.92226076355,532.005992326412,532.085826164877,532.169572897579,532.253216574595,
532.336777318661,532.420275180618,532.50373768118,532.587182816672,532.670628651515,
532.754093246753,532.837646432175,532.921244265748,533.004975828609,533.084809667076,
533.168556399778,533.252200076794,533.335760820861,533.419258682817,533.50272118338,
533.586166318872,533.669612153715,533.753076748953,533.836629934375,533.920227767948,
534.00395933081,534.083793169275,534.167539901977,534.251183578993,534.334744323059,
534.418242185016,534.501704685579,534.585149821071,534.668595655914,534.752060251152,
534.835613436574,534.919211270147,535.002942833009,535.082776671475,535.166523404177,
535.250167081193,535.333727825259,535.417225687216,535.500688187779,535.584133323271,
535.667579158114,535.751043753352,535.834596938774,535.918194772347,536.001926335209,
536.081760173674,536.165506906376,536.249150583392,536.332711327458,536.416209189415,
536.499671689977,536.58311682547,536.666562660312,536.75002725555,536.833580440972,
536.917178274545,537.000909837407,537.080743675873,537.212343763855),
 .UNSPECIFIED.);
#499=B_SPLINE_CURVE_WITH_KNOTS('',3,(#64981,#64982,#64983,#64984,#64985,
#64986,#64987,#64988,#64989,#64990,#64991,#64992,#64993,#64994,#64995,#64996,
#64997,#64998,#64999,#65000,#65001,#65002,#65003,#65004,#65005,#65006,#65007,
#65008,#65009,#65010,#65011,#65012,#65013,#65014,#65015,#65016,#65017,#65018,
#65019,#65020,#65021,#65022,#65023,#65024,#65025,#65026,#65027,#65028,#65029,
#65030,#65031,#65032,#65033,#65034,#65035,#65036,#65037,#65038,#65039,#65040,
#65041,#65042,#65043,#65044,#65045,#65046,#65047,#65048,#65049,#65050,#65051,
#65052,#65053,#65054,#65055,#65056,#65057,#65058,#65059,#65060,#65061,#65062,
#65063,#65064,#65065,#65066,#65067,#65068,#65069,#65070,#65071,#65072,#65073,
#65074,#65075,#65076,#65077,#65078,#65079,#65080,#65081,#65082,#65083,#65084,
#65085,#65086,#65087,#65088,#65089,#65090,#65091,#65092,#65093,#65094,#65095,
#65096,#65097,#65098,#65099,#65100,#65101,#65102,#65103,#65104,#65105,#65106,
#65107,#65108,#65109,#65110,#65111,#65112,#65113,#65114,#65115,#65116,#65117,
#65118,#65119,#65120,#65121,#65122,#65123,#65124,#65125,#65126,#65127,#65128,
#65129,#65130,#65131,#65132,#65133,#65134,#65135,#65136,#65137,#65138,#65139,
#65140,#65141,#65142,#65143,#65144,#65145,#65146,#65147,#65148,#65149,#65150,
#65151,#65152,#65153,#65154,#65155,#65156,#65157,#65158,#65159,#65160,#65161,
#65162,#65163,#65164,#65165,#65166,#65167,#65168,#65169,#65170,#65171,#65172,
#65173,#65174,#65175,#65176,#65177,#65178,#65179,#65180,#65181,#65182,#65183,
#65184,#65185,#65186,#65187,#65188,#65189,#65190,#65191,#65192,#65193,#65194,
#65195,#65196,#65197,#65198,#65199,#65200,#65201,#65202,#65203,#65204,#65205,
#65206,#65207,#65208,#65209),.UNSPECIFIED.,.F.,.F.,(4,3,3,3,3,3,3,3,3,3,
3,3,3,3,3,3,3,3,3,3,3,3,3,3,3,3,3,3,3,3,3,3,3,3,3,3,3,3,3,3,3,3,3,3,3,3,
3,3,3,3,3,3,3,3,3,3,3,3,3,3,3,3,3,3,3,3,3,3,3,3,3,3,3,3,3,3,4),(537.212343763982,
537.2948206532,537.377211365898,537.459537018521,537.541825304515,537.624096120113,
537.706368459933,537.788661317575,537.871040033356,537.953466747926,538.036014048594,
538.079727178072,538.163473910774,538.24711758779,538.330678331856,538.414176193813,
538.497638694375,538.581083829868,538.66452966471,538.747994259949,538.83154744537,
538.915145278943,538.998876841805,539.078710680271,539.162457412973,539.246101089989,
539.329661834056,539.413159696012,539.496622196575,539.580067332067,539.66351316691,
539.746977762148,539.83053094757,539.914128781143,539.997860344005,540.07769418247,
540.161440915172,540.245084592188,540.328645336255,540.412143198212,540.495605698774,
540.579050834266,540.662496669109,540.745961264347,540.829514449769,540.913112283342,
540.996843846204,541.07667768467,541.160424417372,541.244068094388,541.327628838455,
541.411126700412,541.494589200974,541.578034336467,541.66148017131,541.744944766548,
541.82849795197,541.912095785542,541.995827348404,542.075661186869,542.159407919571,
542.243051596586,542.326612340653,542.41011020261,542.493572703173,542.577017838665,
542.660463673508,542.743928268745,542.827481454167,542.91107928774,542.994810850602,
543.074644689068,543.166514762158,543.258040747508,543.349348384809,543.440308855984,
543.495529070882),.UNSPECIFIED.);
#500=B_SPLINE_CURVE_WITH_KNOTS('',3,(#65211,#65212,#65213,#65214,#65215,
#65216,#65217,#65218,#65219,#65220,#65221,#65222,#65223,#65224,#65225,#65226,
#65227,#65228,#65229,#65230,#65231,#65232,#65233,#65234,#65235,#65236,#65237,
#65238,#65239,#65240,#65241,#65242,#65243,#65244,#65245,#65246,#65247,#65248,
#65249,#65250,#65251,#65252,#65253,#65254,#65255,#65256,#65257,#65258,#65259,
#65260,#65261,#65262,#65263,#65264,#65265,#65266,#65267,#65268,#65269,#65270,
#65271,#65272,#65273,#65274,#65275,#65276,#65277,#65278,#65279,#65280,#65281,
#65282,#65283,#65284,#65285,#65286,#65287,#65288,#65289,#65290,#65291,#65292,
#65293,#65294,#65295,#65296,#65297,#65298,#65299,#65300,#65301,#65302,#65303,
#65304,#65305,#65306,#65307,#65308,#65309,#65310,#65311,#65312,#65313,#65314,
#65315,#65316,#65317,#65318,#65319,#65320,#65321,#65322,#65323,#65324,#65325,
#65326,#65327,#65328,#65329,#65330,#65331,#65332,#65333,#65334,#65335,#65336,
#65337,#65338,#65339,#65340,#65341,#65342,#65343,#65344,#65345,#65346,#65347,
#65348,#65349,#65350,#65351,#65352,#65353,#65354,#65355,#65356,#65357,#65358,
#65359,#65360,#65361,#65362,#65363,#65364,#65365,#65366,#65367,#65368,#65369,
#65370,#65371,#65372,#65373,#65374,#65375,#65376,#65377,#65378,#65379,#65380,
#65381,#65382,#65383,#65384,#65385,#65386,#65387,#65388,#65389,#65390,#65391,
#65392,#65393,#65394,#65395,#65396,#65397,#65398,#65399,#65400,#65401,#65402,
#65403,#65404,#65405,#65406,#65407,#65408,#65409,#65410,#65411,#65412,#65413,
#65414,#65415,#65416,#65417,#65418,#65419,#65420,#65421,#65422,#65423,#65424,
#65425,#65426,#65427,#65428,#65429,#65430,#65431,#65432,#65433,#65434,#65435,
#65436,#65437,#65438,#65439),.UNSPECIFIED.,.F.,.F.,(4,3,3,3,3,3,3,3,3,3,
3,3,3,3,3,3,3,3,3,3,3,3,3,3,3,3,3,3,3,3,3,3,3,3,3,3,3,3,3,3,3,3,3,3,3,3,
3,3,3,3,3,3,3,3,3,3,3,3,3,3,3,3,3,3,3,3,3,3,3,3,3,3,3,3,3,3,4),(543.495529071034,
543.580585919541,543.665679585698,543.750825481719,543.836101155191,543.921445673897,
544.00694746502,544.073628191267,544.157374923969,544.241018600984,544.324579345051,
544.408077207008,544.49153970757,544.574984843062,544.658430677905,544.741895273143,
544.825448458564,544.909046292137,544.992777854998,545.072611693466,545.156358426168,
545.240002103184,545.32356284725,545.407060709207,545.490523209769,545.573968345261,
545.657414180104,545.740878775342,545.824431960764,545.908029794336,545.991761357198,
546.071595195665,546.155341928368,546.238985605384,546.322546349451,546.406044211407,
546.48950671197,546.572951847463,546.656397682306,546.739862277544,546.823415462967,
546.90701329654,546.990744859402,547.070578697865,547.154325430567,547.237969107583,
547.321529851649,547.405027713606,547.488490214169,547.571935349661,547.655381184504,
547.738845779743,547.822398965164,547.905996798737,547.989728361599,548.069562200064,
548.153308932766,548.236952609781,548.320513353848,548.404011215804,548.487473716366,
548.570918851859,548.654364686701,548.737829281939,548.821382467361,548.904980300933,
548.988711863795,549.068545702263,549.151692740348,549.234706332708,549.317642823717,
549.400520897003,549.483359188964,549.566191689685,549.649019764715,549.731889025188,
549.778714378214),.UNSPECIFIED.);
#501=B_SPLINE_CURVE_WITH_KNOTS('',3,(#65441,#65442,#65443,#65444,#65445,
#65446,#65447,#65448,#65449,#65450,#65451),.UNSPECIFIED.,.F.,.F.,(4,1,1,
1,1,1,2,4),(549.77871935695,550.067529204462,551.066512706661,552.065496208861,
553.06447971106,554.063463213259,555.062446715458,556.061899685393),
 .UNSPECIFIED.);
#502=B_SPLINE_CURVE_WITH_KNOTS('',3,(#65453,#65454,#65455,#65456,#65457,
#65458,#65459,#65460,#65461,#65462),.UNSPECIFIED.,.F.,.F.,(4,1,1,1,1,1,
1,4),(556.061899685393,557.060413719856,558.059397222055,559.058380724255,
560.057364226454,561.056347728653,562.055331230852,562.345079947443),
 .UNSPECIFIED.);
#503=B_SPLINE_CURVE_WITH_KNOTS('',3,(#65464,#65465,#65466,#65467,#65468,
#65469,#65470,#65471,#65472,#65473,#65474,#65475,#65476,#65477,#65478,#65479,
#65480,#65481,#65482,#65483,#65484,#65485,#65486,#65487,#65488,#65489,#65490,
#65491,#65492,#65493,#65494,#65495,#65496,#65497,#65498,#65499,#65500,#65501,
#65502,#65503,#65504,#65505,#65506,#65507,#65508,#65509,#65510,#65511,#65512,
#65513,#65514,#65515,#65516,#65517,#65518,#65519,#65520,#65521,#65522,#65523,
#65524,#65525,#65526,#65527,#65528,#65529,#65530,#65531,#65532,#65533,#65534,
#65535,#65536,#65537,#65538,#65539,#65540,#65541,#65542,#65543,#65544,#65545,
#65546,#65547,#65548,#65549,#65550,#65551,#65552,#65553,#65554,#65555,#65556,
#65557,#65558,#65559,#65560,#65561,#65562,#65563,#65564,#65565,#65566,#65567,
#65568,#65569,#65570,#65571,#65572,#65573,#65574,#65575,#65576,#65577,#65578,
#65579,#65580,#65581,#65582,#65583,#65584,#65585,#65586,#65587,#65588,#65589,
#65590,#65591,#65592,#65593,#65594,#65595,#65596,#65597,#65598,#65599,#65600,
#65601,#65602,#65603,#65604,#65605,#65606,#65607,#65608,#65609,#65610,#65611,
#65612,#65613,#65614,#65615,#65616,#65617,#65618,#65619,#65620,#65621,#65622,
#65623,#65624,#65625,#65626,#65627,#65628,#65629,#65630,#65631,#65632,#65633,
#65634,#65635,#65636,#65637,#65638,#65639,#65640,#65641,#65642,#65643,#65644,
#65645,#65646,#65647,#65648,#65649,#65650,#65651,#65652,#65653,#65654,#65655,
#65656,#65657,#65658,#65659,#65660,#65661,#65662,#65663,#65664,#65665,#65666,
#65667,#65668,#65669,#65670,#65671,#65672,#65673,#65674,#65675,#65676,#65677,
#65678,#65679,#65680,#65681,#65682,#65683,#65684,#65685,#65686,#65687,#65688,
#65689,#65690,#65691,#65692),.UNSPECIFIED.,.F.,.F.,(4,3,3,3,3,3,3,3,3,3,
3,3,3,3,3,3,3,3,3,3,3,3,3,3,3,3,3,3,3,3,3,3,3,3,3,3,3,3,3,3,3,3,3,3,3,3,
3,3,3,3,3,3,3,3,3,3,3,3,3,3,3,3,3,3,3,3,3,3,3,3,3,3,3,3,3,3,4),(562.345084992573,
562.427965235509,562.510816580263,562.593655547536,562.676500711991,562.759370649371,
562.842332057276,562.925344429649,563.008481840182,563.054314733051,563.138061465753,
563.221705142769,563.305265886835,563.388763748792,563.472226249355,563.555671384847,
563.63911721969,563.722581814928,563.80613500035,563.889732833922,563.973464396784,
564.05329823525,564.137044967952,564.220688644968,564.304249389034,564.387747250991,
564.471209751554,564.554654887046,564.638100721889,564.721565317127,564.805118502549,
564.888716336121,564.972447898983,565.05228173745,565.136028470152,565.219672147168,
565.303232891235,565.386730753191,565.470193253754,565.553638389247,565.63708422409,
565.720548819328,565.80410200475,565.887699838323,565.971431401185,566.051265239649,
566.135011972351,566.218655649366,566.302216393433,566.38571425539,566.469176755952,
566.552621891444,566.636067726287,566.719532321525,566.803085506947,566.886683340519,
566.970414903381,567.050248741848,567.13399547455,567.217639151566,567.301199895632,
567.384697757589,567.468160258151,567.551605393644,567.635051228487,567.718515823725,
567.802069009147,567.885666842719,567.969398405581,568.049232244047,568.134713532804,
568.220077174772,568.305338890218,568.390493180076,568.475584384095,568.560622501914,
568.628270299753),.UNSPECIFIED.);
#504=B_SPLINE_CURVE_WITH_KNOTS('',3,(#65694,#65695,#65696,#65697,#65698,
#65699,#65700,#65701,#65702,#65703,#65704,#65705,#65706,#65707,#65708,#65709,
#65710,#65711,#65712,#65713,#65714,#65715,#65716,#65717,#65718,#65719,#65720,
#65721,#65722,#65723,#65724,#65725,#65726,#65727,#65728,#65729,#65730,#65731,
#65732,#65733,#65734,#65735,#65736,#65737,#65738,#65739,#65740,#65741,#65742,
#65743,#65744,#65745,#65746,#65747,#65748,#65749,#65750,#65751,#65752,#65753,
#65754,#65755,#65756,#65757,#65758,#65759,#65760,#65761,#65762,#65763,#65764,
#65765,#65766,#65767,#65768,#65769,#65770,#65771,#65772,#65773,#65774,#65775,
#65776,#65777,#65778,#65779,#65780,#65781,#65782,#65783,#65784,#65785,#65786,
#65787,#65788,#65789,#65790,#65791,#65792,#65793,#65794,#65795,#65796,#65797,
#65798,#65799,#65800,#65801,#65802,#65803,#65804,#65805,#65806,#65807,#65808,
#65809,#65810,#65811,#65812,#65813,#65814,#65815,#65816,#65817,#65818,#65819,
#65820,#65821,#65822,#65823,#65824,#65825,#65826,#65827,#65828,#65829,#65830,
#65831,#65832,#65833,#65834,#65835,#65836,#65837,#65838,#65839,#65840,#65841,
#65842,#65843,#65844,#65845,#65846,#65847,#65848,#65849,#65850,#65851,#65852,
#65853,#65854,#65855,#65856,#65857,#65858,#65859,#65860,#65861,#65862,#65863,
#65864,#65865,#65866,#65867,#65868,#65869,#65870,#65871,#65872,#65873,#65874,
#65875,#65876,#65877,#65878,#65879,#65880,#65881,#65882,#65883,#65884,#65885,
#65886,#65887,#65888,#65889,#65890,#65891,#65892,#65893,#65894,#65895,#65896,
#65897,#65898,#65899,#65900,#65901,#65902,#65903,#65904,#65905,#65906,#65907,
#65908,#65909,#65910,#65911,#65912,#65913,#65914,#65915,#65916,#65917,#65918,
#65919,#65920,#65921,#65922),.UNSPECIFIED.,.F.,.F.,(4,3,3,3,3,3,3,3,3,3,
3,3,3,3,3,3,3,3,3,3,3,3,3,3,3,3,3,3,3,3,3,3,3,3,3,3,3,3,3,3,3,3,3,3,3,3,
3,3,3,3,3,3,3,3,3,3,3,3,3,3,3,3,3,3,3,3,3,3,3,3,3,3,3,3,3,3,4),(568.62827029991,
568.71920626783,568.810556815388,568.902118985271,568.993991397215,569.048215746246,
569.131962478948,569.215606155964,569.29916690003,569.382664761987,569.46612726255,
569.549572398042,569.633018232885,569.716482828123,569.800036013545,569.883633847117,
569.967365409979,570.047199248445,570.130945981147,570.214589658163,570.298150402229,
570.381648264186,570.465110764749,570.548555900241,570.632001735084,570.715466330322,
570.799019515744,570.882617349317,570.966348912179,571.046182750645,571.129929483347,
571.213573160363,571.29713390443,571.380631766386,571.464094266949,571.547539402442,
571.630985237284,571.714449832523,571.798003017945,571.881600851517,571.965332414379,
572.045166252844,572.128912985546,572.212556662562,572.296117406628,572.379615268585,
572.463077769147,572.546522904639,572.629968739482,572.71343333472,572.796986520142,
572.880584353715,572.964315916576,573.044149755043,573.127896487745,573.211540164761,
573.295100908827,573.378598770784,573.462061271346,573.545506406839,573.628952241681,
573.712416836919,573.795970022341,573.879567855914,573.963299418775,574.043133257242,
574.12569152221,574.208147557982,574.29052255149,574.372836281538,574.455117716533,
574.537385860219,574.619659702699,574.701997233827,574.784370000703,574.866844481791,
574.911455606805),.UNSPECIFIED.);
#505=B_SPLINE_CURVE_WITH_KNOTS('',3,(#65924,#65925,#65926,#65927,#65928,
#65929,#65930,#65931,#65932,#65933,#65934,#65935,#65936,#65937,#65938,#65939,
#65940,#65941,#65942,#65943,#65944,#65945,#65946,#65947,#65948,#65949,#65950,
#65951,#65952,#65953,#65954,#65955,#65956,#65957,#65958,#65959,#65960,#65961,
#65962,#65963,#65964,#65965,#65966,#65967,#65968,#65969,#65970,#65971,#65972,
#65973,#65974,#65975,#65976,#65977,#65978,#65979,#65980,#65981,#65982,#65983,
#65984,#65985,#65986,#65987,#65988,#65989,#65990,#65991,#65992,#65993,#65994,
#65995,#65996,#65997,#65998,#65999,#66000,#66001,#66002,#66003,#66004,#66005,
#66006,#66007,#66008,#66009,#66010,#66011,#66012,#66013,#66014,#66015,#66016,
#66017,#66018,#66019,#66020,#66021,#66022,#66023,#66024,#66025,#66026,#66027,
#66028,#66029,#66030,#66031,#66032,#66033,#66034,#66035,#66036,#66037,#66038,
#66039,#66040,#66041,#66042,#66043,#66044,#66045,#66046,#66047,#66048,#66049,
#66050,#66051,#66052,#66053,#66054,#66055,#66056,#66057,#66058,#66059,#66060,
#66061,#66062,#66063,#66064,#66065,#66066,#66067,#66068,#66069,#66070,#66071,
#66072,#66073,#66074,#66075,#66076,#66077,#66078,#66079,#66080,#66081,#66082,
#66083,#66084,#66085,#66086,#66087,#66088,#66089,#66090,#66091,#66092,#66093,
#66094,#66095,#66096,#66097,#66098,#66099,#66100,#66101,#66102,#66103,#66104,
#66105,#66106,#66107,#66108,#66109,#66110,#66111,#66112,#66113,#66114,#66115,
#66116,#66117,#66118,#66119,#66120,#66121,#66122,#66123,#66124,#66125,#66126,
#66127,#66128,#66129,#66130,#66131,#66132,#66133,#66134,#66135,#66136,#66137,
#66138,#66139,#66140,#66141,#66142,#66143,#66144,#66145,#66146,#66147,#66148,
#66149),.UNSPECIFIED.,.F.,.F.,(4,3,3,3,3,3,3,3,3,3,3,3,3,3,3,3,3,3,3,3,
3,3,3,3,3,3,3,3,3,3,3,3,3,3,3,3,3,3,3,3,3,3,3,3,3,3,3,3,3,3,3,3,3,3,3,3,
3,3,3,3,3,3,3,3,3,3,3,3,3,3,3,3,3,3,3,4),(574.911455606932,575.042116759441,
575.125863492143,575.209507169159,575.293067913225,575.376565775182,575.460028275744,
575.543473411236,575.626919246079,575.710383841317,575.793937026739,575.877534860312,
575.961266423173,576.04110026164,576.124846994342,576.208490671358,576.292051415424,
576.375549277381,576.459011777944,576.542456913436,576.625902748279,576.709367343517,
576.792920528939,576.876518362511,576.960249925373,577.040083763839,577.123830496541,
577.207474173557,577.291034917624,577.374532779581,577.457995280143,577.541440415636,
577.624886250479,577.708350845717,577.791904031139,577.875501864712,577.959233427574,
578.039067266039,578.122813998741,578.206457675757,578.290018419823,578.37351628178,
578.456978782342,578.540423917834,578.623869752677,578.707334347915,578.790887533337,
578.87448536691,578.958216929771,579.038050768238,579.12179750094,579.205441177956,
579.289001922022,579.372499783979,579.455962284542,579.539407420034,579.622853254877,
579.706317850115,579.789871035536,579.873468869109,579.957200431971,580.037034270437,
580.120781003139,580.204424680155,580.287985424221,580.371483286178,580.454945786741,
580.538390922233,580.621836757076,580.705301352314,580.788854537735,580.872452371308,
580.95618393417,581.036017772636,581.173030216201,581.194640914112),
 .UNSPECIFIED.);
#506=B_SPLINE_CURVE_WITH_KNOTS('',3,(#66151,#66152,#66153,#66154,#66155,
#66156,#66157,#66158,#66159,#66160,#66161,#66162,#66163,#66164,#66165,#66166,
#66167,#66168,#66169,#66170,#66171,#66172,#66173,#66174,#66175,#66176,#66177,
#66178,#66179,#66180,#66181,#66182,#66183,#66184,#66185,#66186,#66187,#66188,
#66189,#66190,#66191,#66192,#66193,#66194,#66195,#66196,#66197,#66198,#66199,
#66200,#66201,#66202,#66203,#66204,#66205,#66206,#66207,#66208,#66209,#66210,
#66211,#66212,#66213,#66214,#66215,#66216,#66217,#66218,#66219,#66220,#66221,
#66222,#66223,#66224,#66225,#66226,#66227,#66228,#66229,#66230,#66231,#66232,
#66233,#66234,#66235,#66236,#66237,#66238,#66239,#66240,#66241,#66242,#66243,
#66244,#66245,#66246,#66247,#66248,#66249,#66250,#66251,#66252,#66253,#66254,
#66255,#66256,#66257,#66258,#66259,#66260,#66261,#66262,#66263,#66264,#66265,
#66266,#66267,#66268,#66269,#66270,#66271,#66272,#66273,#66274,#66275,#66276,
#66277,#66278,#66279,#66280,#66281,#66282,#66283,#66284,#66285,#66286,#66287,
#66288,#66289,#66290,#66291,#66292,#66293,#66294,#66295,#66296,#66297,#66298,
#66299,#66300,#66301,#66302,#66303,#66304,#66305,#66306,#66307,#66308,#66309,
#66310,#66311,#66312,#66313,#66314,#66315,#66316,#66317,#66318,#66319,#66320,
#66321,#66322,#66323,#66324,#66325,#66326,#66327,#66328,#66329,#66330,#66331,
#66332,#66333,#66334,#66335,#66336,#66337,#66338,#66339,#66340,#66341,#66342,
#66343,#66344,#66345,#66346,#66347,#66348,#66349,#66350,#66351,#66352,#66353,
#66354,#66355,#66356,#66357,#66358,#66359,#66360,#66361,#66362,#66363,#66364,
#66365,#66366,#66367,#66368,#66369,#66370,#66371,#66372,#66373,#66374,#66375,
#66376,#66377,#66378,#66379),.UNSPECIFIED.,.F.,.F.,(4,3,3,3,3,3,3,3,3,3,
3,3,3,3,3,3,3,3,3,3,3,3,3,3,3,3,3,3,3,3,3,3,3,3,3,3,3,3,3,3,3,3,3,3,3,3,
3,3,3,3,3,3,3,3,3,3,3,3,3,3,3,3,3,3,3,3,3,3,3,3,3,3,3,3,3,3,4),(581.194640914215,
581.277035727267,581.35935063523,581.443806965181,581.526033315061,581.608248433236,
581.690471345369,581.776603827735,581.858944381822,581.941339481402,582.023846563504,
582.035001274835,582.118748007537,582.202391684552,582.285952428619,582.369450290576,
582.452912791138,582.53635792663,582.619803761473,582.703268356711,582.786821542133,
582.870419375705,582.954150938567,583.033984777034,583.117731509736,583.201375186752,
583.284935930819,583.368433792775,583.451896293338,583.535341428831,583.618787263674,
583.702251858912,583.785805044334,583.869402877907,583.953134440769,584.032968279234,
584.116715011936,584.200358688952,584.283919433019,584.367417294976,584.450879795538,
584.534324931031,584.617770765874,584.701235361112,584.784788546534,584.868386380106,
584.952117942968,585.031951781433,585.115698514135,585.19934219115,585.282902935216,
585.366400797173,585.449863297735,585.533308433227,585.61675426807,585.700218863308,
585.783772048729,585.867369882302,585.951101445163,586.030935283632,586.114682016334,
586.19832569335,586.281886437417,586.365384299373,586.448846799936,586.532291935428,
586.615737770271,586.699202365509,586.782755550931,586.866353384504,586.950084947366,
587.029918785831,587.120300133636,587.210388364691,587.300299953113,587.389929836687,
587.477826221184),.UNSPECIFIED.);
#507=B_SPLINE_CURVE_WITH_KNOTS('',3,(#66381,#66382,#66383,#66384,#66385,
#66386,#66387,#66388,#66389,#66390,#66391,#66392,#66393,#66394,#66395,#66396,
#66397,#66398,#66399,#66400,#66401,#66402,#66403,#66404,#66405,#66406,#66407,
#66408,#66409,#66410,#66411,#66412,#66413,#66414,#66415,#66416,#66417,#66418,
#66419,#66420,#66421,#66422,#66423,#66424,#66425,#66426,#66427,#66428,#66429,
#66430,#66431,#66432,#66433,#66434,#66435,#66436,#66437,#66438,#66439,#66440,
#66441,#66442,#66443,#66444,#66445,#66446,#66447,#66448,#66449,#66450,#66451,
#66452,#66453,#66454,#66455,#66456,#66457,#66458,#66459,#66460,#66461,#66462,
#66463,#66464,#66465,#66466,#66467,#66468,#66469,#66470,#66471,#66472,#66473,
#66474,#66475,#66476,#66477,#66478,#66479,#66480,#66481,#66482,#66483,#66484,
#66485,#66486,#66487,#66488,#66489,#66490,#66491,#66492,#66493,#66494,#66495,
#66496,#66497,#66498,#66499,#66500,#66501,#66502,#66503,#66504,#66505,#66506,
#66507,#66508,#66509,#66510,#66511,#66512,#66513,#66514,#66515,#66516,#66517,
#66518,#66519,#66520,#66521,#66522,#66523,#66524,#66525,#66526,#66527,#66528,
#66529,#66530,#66531,#66532,#66533,#66534,#66535,#66536,#66537,#66538,#66539,
#66540,#66541,#66542,#66543,#66544,#66545,#66546,#66547,#66548,#66549,#66550,
#66551,#66552,#66553,#66554,#66555,#66556,#66557,#66558,#66559,#66560,#66561,
#66562,#66563,#66564,#66565,#66566,#66567,#66568,#66569,#66570,#66571,#66572,
#66573,#66574,#66575,#66576,#66577,#66578,#66579,#66580,#66581,#66582,#66583,
#66584,#66585,#66586,#66587,#66588,#66589,#66590,#66591,#66592,#66593,#66594,
#66595,#66596,#66597,#66598,#66599,#66600,#66601,#66602,#66603,#66604,#66605,
#66606,#66607,#66608,#66609),.UNSPECIFIED.,.F.,.F.,(4,3,3,3,3,3,3,3,3,3,
3,3,3,3,3,3,3,3,3,3,3,3,3,3,3,3,3,3,3,3,3,3,3,3,3,3,3,3,3,3,3,3,3,3,3,3,
3,3,3,3,3,3,3,3,3,3,3,3,3,3,3,3,3,3,3,3,3,3,3,3,3,3,3,3,3,3,4),(587.477826221291,
587.563586830846,587.649406073758,587.735297697654,587.82133727072,587.907460242967,
587.993739923875,588.02890228803,588.112649020733,588.196292697749,588.279853441816,
588.363351303773,588.446813804336,588.530258939828,588.613704774672,588.69716936991,
588.780722555333,588.864320388906,588.948051951768,589.02788579023,589.111632522932,
589.195276199948,589.278836944014,589.362334805971,589.445797306534,589.529242442026,
589.612688276869,589.696152872106,589.779706057528,589.863303891101,589.947035453962,
590.026869292429,590.110616025131,590.194259702147,590.277820446213,590.36131830817,
590.444780808732,590.528225944224,590.611671779067,590.695136374305,590.778689559727,
590.8622873933,590.946018956162,591.025852794628,591.10959952733,591.193243204346,
591.276803948412,591.360301810369,591.443764310932,591.527209446424,591.610655281267,
591.694119876505,591.777673061926,591.861270895499,591.945002458361,592.024836296827,
592.108583029529,592.192226706545,592.275787450611,592.359285312567,592.44274781313,
592.526192948622,592.609638783465,592.693103378703,592.776656564124,592.860254397697,
592.943985960559,593.023819799026,593.106705162984,593.18946020447,593.272140356324,
593.354764495462,593.437351451291,593.519941160403,593.602528724221,593.685173429262,
593.761011528471),.UNSPECIFIED.);
#508=B_SPLINE_CURVE_WITH_KNOTS('',3,(#66611,#66612,#66613,#66614,#66615,
#66616,#66617,#66618,#66619,#66620,#66621,#66622,#66623,#66624,#66625,#66626,
#66627,#66628,#66629,#66630,#66631,#66632,#66633,#66634,#66635,#66636,#66637,
#66638,#66639,#66640,#66641,#66642,#66643,#66644,#66645,#66646,#66647,#66648,
#66649,#66650,#66651,#66652,#66653,#66654,#66655,#66656,#66657,#66658,#66659,
#66660,#66661,#66662,#66663,#66664,#66665,#66666,#66667,#66668,#66669,#66670,
#66671,#66672,#66673,#66674,#66675,#66676,#66677,#66678,#66679,#66680,#66681,
#66682,#66683,#66684,#66685,#66686,#66687,#66688,#66689,#66690,#66691,#66692,
#66693,#66694,#66695,#66696,#66697,#66698,#66699,#66700,#66701,#66702,#66703,
#66704,#66705,#66706,#66707,#66708,#66709,#66710,#66711,#66712,#66713,#66714,
#66715,#66716,#66717,#66718,#66719,#66720,#66721,#66722,#66723,#66724,#66725,
#66726,#66727,#66728,#66729,#66730,#66731,#66732,#66733,#66734,#66735,#66736,
#66737,#66738,#66739,#66740,#66741,#66742,#66743,#66744,#66745,#66746,#66747,
#66748,#66749,#66750,#66751,#66752,#66753,#66754,#66755,#66756,#66757,#66758,
#66759,#66760,#66761,#66762,#66763,#66764,#66765,#66766,#66767,#66768,#66769,
#66770,#66771,#66772,#66773,#66774,#66775,#66776,#66777,#66778,#66779,#66780,
#66781,#66782,#66783,#66784,#66785,#66786,#66787,#66788,#66789,#66790,#66791,
#66792,#66793,#66794,#66795,#66796,#66797,#66798,#66799,#66800,#66801,#66802,
#66803,#66804,#66805,#66806,#66807,#66808,#66809,#66810,#66811,#66812,#66813,
#66814,#66815,#66816,#66817,#66818,#66819,#66820,#66821,#66822,#66823,#66824,
#66825,#66826,#66827,#66828,#66829,#66830,#66831,#66832,#66833,#66834,#66835,
#66836,#66837,#66838,#66839),.UNSPECIFIED.,.F.,.F.,(4,3,3,3,3,3,3,3,3,3,
3,3,3,3,3,3,3,3,3,3,3,3,3,3,3,3,3,3,3,3,3,3,3,3,3,3,3,3,3,3,3,3,3,3,3,3,
3,3,3,3,3,3,3,3,3,3,3,3,3,3,3,3,3,3,3,3,3,3,3,3,3,3,3,3,3,3,4),(593.761011528614,
593.866374367455,593.973784241142,594.022803301225,594.106550033927,594.190193710943,
594.27375445501,594.357252316966,594.440714817529,594.524159953021,594.607605787864,
594.691070383102,594.774623568524,594.858221402097,594.941952964959,595.021786803424,
595.105533536126,595.189177213142,595.272737957209,595.356235819165,595.439698319728,
595.52314345522,595.606589290063,595.690053885301,595.773607070723,595.857204904296,
595.940936467158,596.020770305624,596.104517038326,596.188160715342,596.271721459408,
596.355219321365,596.438681821928,596.52212695742,596.605572792263,596.689037387501,
596.772590572923,596.856188406496,596.939919969358,597.019753807823,597.103500540525,
597.187144217541,597.270704961607,597.354202823564,597.437665324127,597.521110459619,
597.604556294462,597.6880208897,597.771574075122,597.855171908694,597.938903471556,
598.018737310022,598.102484042724,598.18612771974,598.269688463806,598.353186325763,
598.436648826325,598.520093961817,598.60353979666,598.687004391898,598.77055757732,
598.854155410893,598.937886973754,599.017720812221,599.101467544923,599.185111221939,
599.268671966005,599.352169827962,599.435632328525,599.519077464017,599.60252329886,
599.685987894098,599.76954107952,599.853138913093,599.936870475955,600.01670431442,
600.04419683565),.UNSPECIFIED.);
#509=B_SPLINE_CURVE_WITH_KNOTS('',3,(#66841,#66842,#66843,#66844,#66845,
#66846,#66847,#66848,#66849,#66850,#66851,#66852,#66853,#66854,#66855,#66856,
#66857,#66858,#66859,#66860,#66861,#66862,#66863,#66864,#66865,#66866,#66867,
#66868,#66869,#66870,#66871,#66872,#66873,#66874,#66875,#66876,#66877,#66878,
#66879,#66880,#66881,#66882,#66883,#66884,#66885,#66886,#66887,#66888,#66889,
#66890,#66891,#66892,#66893,#66894,#66895,#66896,#66897,#66898,#66899,#66900,
#66901,#66902,#66903,#66904,#66905,#66906,#66907,#66908,#66909,#66910,#66911,
#66912,#66913,#66914,#66915,#66916,#66917,#66918,#66919,#66920,#66921,#66922,
#66923,#66924,#66925,#66926,#66927,#66928,#66929,#66930,#66931,#66932,#66933,
#66934,#66935,#66936,#66937,#66938,#66939,#66940,#66941,#66942,#66943,#66944,
#66945,#66946,#66947,#66948,#66949,#66950,#66951,#66952,#66953,#66954,#66955,
#66956,#66957,#66958,#66959,#66960,#66961,#66962,#66963,#66964,#66965,#66966,
#66967,#66968,#66969,#66970,#66971,#66972,#66973,#66974,#66975,#66976,#66977,
#66978,#66979,#66980,#66981,#66982,#66983,#66984,#66985,#66986,#66987,#66988,
#66989,#66990,#66991,#66992,#66993,#66994,#66995,#66996,#66997,#66998,#66999,
#67000,#67001,#67002,#67003,#67004,#67005,#67006,#67007,#67008,#67009,#67010,
#67011,#67012,#67013,#67014,#67015,#67016,#67017,#67018,#67019,#67020,#67021,
#67022,#67023,#67024,#67025,#67026,#67027,#67028,#67029,#67030,#67031,#67032,
#67033,#67034,#67035,#67036,#67037,#67038,#67039,#67040,#67041,#67042,#67043,
#67044,#67045,#67046,#67047,#67048,#67049,#67050,#67051,#67052,#67053,#67054,
#67055,#67056,#67057,#67058,#67059,#67060,#67061,#67062,#67063,#67064,#67065,
#67066,#67067,#67068,#67069),.UNSPECIFIED.,.F.,.F.,(4,3,3,3,3,3,3,3,3,3,
3,3,3,3,3,3,3,3,3,3,3,3,3,3,3,3,3,3,3,3,3,3,3,3,3,3,3,3,3,3,3,3,3,3,3,3,
3,3,3,3,3,3,3,3,3,3,3,3,3,3,3,3,3,3,3,3,3,3,3,3,3,3,3,3,3,3,4),(600.044196835773,
600.127557274234,600.210815756894,600.293992793723,600.377108819792,600.460192280264,
600.543260777893,600.626332723164,600.709426525337,600.79260935285,600.875840271015,
600.959197541668,601.015687816619,601.099434549321,601.183078226337,601.266638970403,
601.35013683236,601.433599332922,601.517044468415,601.600490303258,601.683954898495,
601.767508083917,601.85110591749,601.934837480352,602.014671318819,602.098418051521,
602.182061728537,602.265622472603,602.34912033456,602.432582835123,602.516027970615,
602.599473805458,602.682938400697,602.766491586119,602.850089419691,602.933820982553,
603.013654821018,603.09740155372,603.181045230736,603.264605974802,603.348103836759,
603.431566337322,603.515011472814,603.598457307657,603.681921902895,603.765475088316,
603.849072921889,603.932804484751,604.012638323217,604.096385055919,604.180028732935,
604.263589477001,604.347087338958,604.43054983952,604.513994975012,604.597440809855,
604.680905405093,604.764458590515,604.848056424088,604.93178798695,605.011621825416,
605.095368558118,605.179012235134,605.262572979201,605.346070841158,605.42953334172,
605.512978477213,605.596424312055,605.679888907293,605.763442092715,605.847039926288,
605.93077148915,606.010605327615,606.110691202018,606.210226018898,606.308772913203,
606.327382142661),.UNSPECIFIED.);
#510=B_SPLINE_CURVE_WITH_KNOTS('',3,(#67071,#67072,#67073,#67074,#67075,
#67076,#67077,#67078,#67079,#67080,#67081,#67082,#67083,#67084,#67085,#67086,
#67087,#67088,#67089,#67090,#67091,#67092,#67093,#67094,#67095,#67096,#67097,
#67098,#67099,#67100,#67101,#67102,#67103,#67104,#67105,#67106,#67107,#67108,
#67109,#67110,#67111,#67112,#67113,#67114,#67115,#67116,#67117,#67118,#67119,
#67120,#67121,#67122,#67123,#67124,#67125,#67126,#67127,#67128,#67129,#67130,
#67131,#67132,#67133,#67134,#67135,#67136,#67137,#67138,#67139,#67140,#67141,
#67142,#67143,#67144,#67145,#67146,#67147,#67148,#67149,#67150,#67151,#67152,
#67153,#67154,#67155,#67156,#67157,#67158,#67159,#67160,#67161,#67162,#67163,
#67164,#67165,#67166,#67167,#67168,#67169,#67170,#67171,#67172,#67173,#67174,
#67175,#67176,#67177,#67178,#67179,#67180,#67181,#67182,#67183,#67184,#67185,
#67186,#67187,#67188,#67189,#67190,#67191,#67192,#67193,#67194,#67195,#67196,
#67197,#67198,#67199,#67200,#67201,#67202,#67203,#67204,#67205,#67206,#67207,
#67208,#67209,#67210,#67211,#67212,#67213,#67214,#67215,#67216,#67217,#67218,
#67219,#67220,#67221,#67222,#67223,#67224,#67225,#67226,#67227,#67228,#67229,
#67230,#67231,#67232,#67233,#67234,#67235,#67236,#67237,#67238,#67239,#67240,
#67241,#67242,#67243,#67244,#67245,#67246,#67247,#67248,#67249,#67250,#67251,
#67252,#67253,#67254,#67255,#67256,#67257,#67258,#67259,#67260,#67261,#67262,
#67263,#67264,#67265,#67266,#67267,#67268,#67269,#67270,#67271,#67272,#67273,
#67274,#67275,#67276,#67277,#67278,#67279,#67280,#67281,#67282,#67283,#67284,
#67285,#67286,#67287,#67288,#67289,#67290,#67291,#67292,#67293,#67294,#67295,
#67296,#67297,#67298,#67299,#67300,#67301,#67302),.UNSPECIFIED.,.F.,.F.,
(4,3,3,3,3,3,3,3,3,3,3,3,3,3,3,3,3,3,3,3,3,3,3,3,3,3,3,3,3,3,3,3,3,3,3,
3,3,3,3,3,3,3,3,3,3,3,3,3,3,3,3,3,3,3,3,3,3,3,3,3,3,3,3,3,3,3,3,3,3,3,3,
3,3,3,3,3,3,4),(606.32738214283,606.412657978703,606.495818105016,606.578976589673,
606.662151716541,606.749010994859,606.832321608991,606.915692440895,606.999181171714,
607.009588829814,607.093335562516,607.176979239532,607.260539983599,607.344037845556,
607.427500346118,607.510945481611,607.594391316454,607.677855911692,607.761409097114,
607.845006930686,607.928738493548,608.008572332014,608.092319064716,608.175962741732,
608.259523485799,608.343021347755,608.426483848318,608.50992898381,608.593374818653,
608.676839413891,608.760392599313,608.843990432886,608.927721995748,609.007555834213,
609.091302566915,609.174946243931,609.258506987997,609.342004849953,609.425467350516,
609.508912486008,609.592358320851,609.675822916089,609.759376101511,609.842973935084,
609.926705497945,610.006539336412,610.090286069114,610.173929746129,610.257490490196,
610.340988352152,610.424450852715,610.507895988207,610.59134182305,610.674806418288,
610.75835960371,610.841957437283,610.925689000145,611.005522838611,611.089269571313,
611.172913248329,611.256473992395,611.339971854352,611.423434354915,611.506879490407,
611.59032532525,611.673789920488,611.75734310591,611.840940939483,611.924672502345,
612.00450634081,612.089331029797,612.174044908342,612.25866480143,612.346640463575,
612.431112606904,612.515545829306,612.599957555231,612.61056745001),
 .UNSPECIFIED.);
#511=B_SPLINE_CURVE_WITH_KNOTS('',3,(#67304,#67305,#67306,#67307,#67308,
#67309,#67310,#67311,#67312,#67313,#67314,#67315,#67316,#67317,#67318,#67319,
#67320,#67321,#67322,#67323,#67324,#67325,#67326,#67327,#67328,#67329,#67330,
#67331,#67332,#67333,#67334,#67335,#67336,#67337,#67338,#67339,#67340,#67341,
#67342,#67343,#67344,#67345,#67346,#67347,#67348,#67349,#67350,#67351,#67352,
#67353,#67354,#67355,#67356,#67357,#67358,#67359,#67360,#67361,#67362,#67363,
#67364,#67365,#67366,#67367,#67368,#67369,#67370,#67371,#67372,#67373,#67374,
#67375,#67376,#67377,#67378,#67379,#67380,#67381,#67382,#67383,#67384,#67385,
#67386,#67387,#67388,#67389,#67390,#67391,#67392,#67393,#67394,#67395,#67396,
#67397,#67398,#67399,#67400,#67401,#67402,#67403,#67404,#67405,#67406,#67407,
#67408,#67409,#67410,#67411,#67412,#67413,#67414,#67415,#67416,#67417,#67418,
#67419,#67420,#67421,#67422,#67423,#67424,#67425,#67426,#67427,#67428,#67429,
#67430,#67431,#67432,#67433,#67434,#67435,#67436,#67437,#67438,#67439,#67440,
#67441,#67442,#67443,#67444,#67445,#67446,#67447,#67448,#67449,#67450,#67451,
#67452,#67453,#67454,#67455,#67456,#67457,#67458,#67459,#67460,#67461,#67462,
#67463,#67464,#67465,#67466,#67467,#67468,#67469,#67470,#67471,#67472,#67473,
#67474,#67475,#67476,#67477,#67478,#67479,#67480,#67481,#67482,#67483,#67484,
#67485,#67486,#67487,#67488,#67489,#67490,#67491,#67492,#67493,#67494,#67495,
#67496,#67497,#67498,#67499,#67500,#67501,#67502,#67503,#67504,#67505,#67506,
#67507,#67508,#67509,#67510,#67511,#67512,#67513,#67514,#67515,#67516,#67517,
#67518,#67519,#67520,#67521,#67522,#67523,#67524,#67525,#67526,#67527,#67528,
#67529,#67530,#67531,#67532),.UNSPECIFIED.,.F.,.F.,(4,3,3,3,3,3,3,3,3,3,
3,3,3,3,3,3,3,3,3,3,3,3,3,3,3,3,3,3,3,3,3,3,3,3,3,3,3,3,3,3,3,3,3,3,3,3,
3,3,3,3,3,3,3,3,3,3,3,3,3,3,3,3,3,3,3,3,3,3,3,3,3,3,3,3,3,3,4),(612.610567450196,
612.703061071577,612.796078500098,612.889367888172,612.983000046674,613.003489843009,
613.087236575711,613.170880252728,613.254440996794,613.337938858751,613.421401359314,
613.504846494807,613.58829232965,613.671756924889,613.755310110311,613.838907943884,
613.922639506746,614.002473345209,614.086220077911,614.169863754927,614.253424498993,
614.33692236095,614.420384861513,614.503829997005,614.587275831848,614.670740427086,
614.754293612508,614.83789144608,614.921623008942,615.001456847408,615.08520358011,
615.168847257126,615.252408001192,615.335905863149,615.419368363711,615.502813499204,
615.586259334046,615.669723929284,615.753277114706,615.836874948279,615.920606511141,
616.000440349607,616.084187082309,616.167830759325,616.251391503391,616.334889365348,
616.41835186591,616.501797001402,616.585242836245,616.668707431483,616.752260616905,
616.835858450478,616.919590013339,616.999423851806,617.083170584508,617.166814261524,
617.250375005591,617.333872867547,617.41733536811,617.500780503602,617.584226338445,
617.667690933683,617.751244119105,617.834841952678,617.918573515539,617.998407354005,
618.081085159299,618.163660733751,618.246155174823,618.328588911261,618.41099027326,
618.493378189876,618.575771576746,618.658233567548,618.740730253467,618.823341934791,
618.893752757054),.UNSPECIFIED.);
#512=B_SPLINE_CURVE_WITH_KNOTS('',3,(#67534,#67535,#67536,#67537,#67538,
#67539,#67540,#67541,#67542,#67543,#67544,#67545,#67546,#67547,#67548,#67549,
#67550,#67551,#67552,#67553,#67554,#67555,#67556,#67557,#67558,#67559,#67560,
#67561,#67562,#67563,#67564,#67565,#67566,#67567,#67568,#67569,#67570,#67571,
#67572,#67573,#67574,#67575,#67576,#67577,#67578,#67579,#67580,#67581,#67582,
#67583,#67584,#67585,#67586,#67587,#67588,#67589,#67590,#67591,#67592,#67593,
#67594,#67595,#67596,#67597,#67598,#67599,#67600,#67601,#67602,#67603,#67604,
#67605,#67606,#67607,#67608,#67609,#67610,#67611,#67612,#67613,#67614,#67615,
#67616,#67617,#67618,#67619,#67620,#67621,#67622,#67623,#67624,#67625,#67626,
#67627,#67628,#67629,#67630,#67631,#67632,#67633,#67634,#67635,#67636,#67637,
#67638,#67639,#67640,#67641,#67642,#67643,#67644,#67645,#67646,#67647,#67648,
#67649,#67650,#67651,#67652,#67653,#67654,#67655,#67656,#67657,#67658,#67659,
#67660,#67661,#67662,#67663,#67664,#67665,#67666,#67667,#67668,#67669,#67670,
#67671,#67672,#67673,#67674,#67675,#67676,#67677,#67678,#67679,#67680,#67681,
#67682,#67683,#67684,#67685,#67686,#67687,#67688,#67689,#67690,#67691,#67692,
#67693,#67694,#67695,#67696,#67697,#67698,#67699,#67700,#67701,#67702,#67703,
#67704,#67705,#67706,#67707,#67708,#67709,#67710,#67711,#67712,#67713,#67714,
#67715,#67716,#67717,#67718,#67719,#67720,#67721,#67722,#67723,#67724,#67725,
#67726,#67727,#67728,#67729,#67730,#67731,#67732,#67733,#67734,#67735,#67736,
#67737,#67738,#67739,#67740,#67741,#67742,#67743,#67744,#67745,#67746,#67747,
#67748,#67749,#67750,#67751,#67752,#67753,#67754,#67755,#67756,#67757,#67758,
#67759),.UNSPECIFIED.,.F.,.F.,(4,3,3,3,3,3,3,3,3,3,3,3,3,3,3,3,3,3,3,3,
3,3,3,3,3,3,3,3,3,3,3,3,3,3,3,3,3,3,3,3,3,3,3,3,3,3,3,3,3,3,3,3,3,3,3,3,
3,3,3,3,3,3,3,3,3,3,3,3,3,3,3,3,3,3,3,4),(618.893752757189,618.997390856205,
619.081137588906,619.164781265921,619.248342009987,619.331839871943,619.415302372504,
619.498747507996,619.582193342838,619.665657938075,619.749211123496,619.832808957068,
619.916540519929,619.996374358404,620.080121091106,620.163764768122,620.247325512189,
620.330823374146,620.414285874708,620.497731010201,620.581176845044,620.664641440282,
620.748194625704,620.831792459277,620.915524022139,620.995357860603,621.079104593305,
621.162748270321,621.246309014388,621.329806876344,621.413269376907,621.496714512399,
621.580160347242,621.66362494248,621.747178127902,621.830775961475,621.914507524337,
621.994341362802,622.078088095504,622.161731772519,622.245292516586,622.328790378542,
622.412252879105,622.495698014597,622.579143849439,622.662608444677,622.746161630099,
622.829759463671,622.913491026533,622.993324865001,623.077071597703,623.160715274719,
623.244276018786,623.327773880743,623.411236381306,623.494681516799,623.578127351642,
623.66159194688,623.745145132302,623.828742965875,623.912474528737,623.9923083672,
624.076055099902,624.159698776917,624.243259520983,624.326757382939,624.410219883502,
624.493665018994,624.577110853836,624.660575449074,624.744128634495,624.827726468068,
624.911458030929,624.991291869399,625.116148226334,625.176938064369),
 .UNSPECIFIED.);
#513=B_SPLINE_CURVE_WITH_KNOTS('',3,(#67761,#67762,#67763,#67764,#67765,
#67766,#67767,#67768,#67769,#67770,#67771,#67772,#67773,#67774,#67775,#67776,
#67777,#67778,#67779,#67780,#67781,#67782,#67783,#67784,#67785,#67786,#67787,
#67788,#67789,#67790,#67791,#67792,#67793,#67794,#67795,#67796,#67797,#67798,
#67799,#67800,#67801,#67802,#67803,#67804,#67805,#67806,#67807,#67808,#67809,
#67810,#67811,#67812,#67813,#67814,#67815,#67816,#67817,#67818,#67819,#67820,
#67821,#67822,#67823,#67824,#67825,#67826,#67827,#67828,#67829,#67830,#67831,
#67832,#67833,#67834,#67835,#67836,#67837,#67838,#67839,#67840,#67841,#67842,
#67843,#67844,#67845,#67846,#67847,#67848,#67849,#67850,#67851,#67852,#67853,
#67854,#67855,#67856,#67857,#67858,#67859,#67860,#67861,#67862,#67863,#67864,
#67865,#67866,#67867,#67868,#67869,#67870,#67871,#67872,#67873,#67874,#67875,
#67876,#67877,#67878,#67879,#67880,#67881,#67882,#67883,#67884,#67885,#67886,
#67887,#67888,#67889,#67890,#67891,#67892,#67893,#67894,#67895,#67896,#67897,
#67898,#67899,#67900,#67901,#67902,#67903,#67904,#67905,#67906,#67907,#67908,
#67909,#67910,#67911,#67912,#67913,#67914,#67915,#67916,#67917,#67918,#67919,
#67920,#67921,#67922,#67923,#67924,#67925,#67926,#67927,#67928,#67929,#67930,
#67931,#67932,#67933,#67934,#67935,#67936,#67937,#67938,#67939,#67940,#67941,
#67942,#67943,#67944,#67945,#67946,#67947,#67948,#67949,#67950,#67951,#67952,
#67953,#67954,#67955,#67956,#67957,#67958,#67959,#67960,#67961,#67962,#67963,
#67964,#67965,#67966,#67967,#67968,#67969,#67970,#67971,#67972,#67973,#67974,
#67975,#67976,#67977,#67978,#67979,#67980,#67981,#67982,#67983,#67984,#67985,
#67986,#67987,#67988,#67989),.UNSPECIFIED.,.F.,.F.,(4,3,3,3,3,3,3,3,3,3,
3,3,3,3,3,3,3,3,3,3,3,3,3,3,3,3,3,3,3,3,3,3,3,3,3,3,3,3,3,3,3,3,3,3,3,3,
3,3,3,3,3,3,3,3,3,3,3,3,3,3,3,3,3,3,3,3,3,3,3,3,3,3,3,3,3,3,4),(625.176938064508,
625.259311614705,625.34161229195,625.42386527977,625.50609381087,625.588316912524,
625.670553605361,625.752872415273,625.835233050282,625.917722023103,625.990275371599,
626.074022104303,626.15766578132,626.241226525389,626.324724387348,626.408186887912,
626.491632023406,626.575077858251,626.658542453491,626.742095638914,626.825693472489,
626.909425035352,626.989258873798,627.073005606499,627.156649283513,627.240210027579,
627.323707889534,627.407170390096,627.490615525587,627.574061360429,627.657525955666,
627.741079141087,627.824676974658,627.908408537519,627.988242375997,628.071989108695,
628.155632785706,628.239193529768,628.32269139172,628.406153892279,628.489599027766,
628.573044862605,628.656509457839,628.740062643256,628.823660476825,628.907392039682,
628.987225878196,629.070972610911,629.15461628794,629.238177032019,629.321674893989,
629.405137394565,629.48858253007,629.572028364926,629.655492960177,629.739046145611,
629.822643979196,629.90637554207,629.986209380395,630.069956113086,630.153599790091,
630.237160534146,630.320658396091,630.404120896643,630.487566032125,630.571011866957,
630.654476462184,630.738029647596,630.821627481159,630.905359044011,630.985192882594,
631.074280882029,631.163199898981,631.251887095224,631.340431909341,631.428786118239,
631.460123371444),.UNSPECIFIED.);
#514=B_SPLINE_CURVE_WITH_KNOTS('',3,(#67991,#67992,#67993,#67994,#67995,
#67996,#67997,#67998,#67999,#68000,#68001,#68002,#68003,#68004,#68005,#68006,
#68007,#68008,#68009,#68010,#68011,#68012,#68013,#68014,#68015,#68016,#68017,
#68018,#68019,#68020,#68021,#68022,#68023,#68024,#68025,#68026,#68027,#68028,
#68029,#68030,#68031,#68032,#68033,#68034,#68035,#68036,#68037,#68038,#68039,
#68040,#68041,#68042,#68043,#68044,#68045,#68046,#68047,#68048,#68049,#68050,
#68051,#68052,#68053,#68054,#68055,#68056,#68057,#68058,#68059,#68060,#68061,
#68062,#68063,#68064,#68065,#68066,#68067,#68068,#68069,#68070,#68071,#68072,
#68073,#68074,#68075,#68076,#68077,#68078,#68079,#68080,#68081,#68082,#68083,
#68084,#68085,#68086,#68087,#68088,#68089,#68090,#68091,#68092,#68093,#68094,
#68095,#68096,#68097,#68098,#68099,#68100,#68101,#68102,#68103,#68104,#68105,
#68106,#68107,#68108,#68109,#68110,#68111,#68112,#68113,#68114,#68115,#68116,
#68117,#68118,#68119,#68120,#68121,#68122,#68123,#68124,#68125,#68126,#68127,
#68128,#68129,#68130,#68131,#68132,#68133,#68134,#68135,#68136,#68137,#68138,
#68139,#68140,#68141,#68142,#68143,#68144,#68145,#68146,#68147,#68148,#68149,
#68150,#68151,#68152,#68153,#68154,#68155,#68156,#68157,#68158,#68159,#68160,
#68161,#68162,#68163,#68164,#68165,#68166,#68167,#68168,#68169,#68170,#68171,
#68172,#68173,#68174,#68175,#68176,#68177,#68178,#68179,#68180,#68181,#68182,
#68183,#68184,#68185,#68186,#68187,#68188,#68189,#68190,#68191,#68192,#68193,
#68194,#68195,#68196,#68197,#68198,#68199,#68200,#68201,#68202,#68203,#68204,
#68205,#68206,#68207,#68208,#68209,#68210,#68211,#68212,#68213,#68214,#68215,
#68216,#68217,#68218,#68219),.UNSPECIFIED.,.F.,.F.,(4,3,3,3,3,3,3,3,3,3,
3,3,3,3,3,3,3,3,3,3,3,3,3,3,3,3,3,3,3,3,3,3,3,3,3,3,3,3,3,3,3,3,3,3,3,3,
3,3,3,3,3,3,3,3,3,3,3,3,3,3,3,3,3,3,3,3,3,3,3,3,3,3,3,3,3,3,4),(631.460123371548,
631.546693513228,631.633348853353,631.721055736213,631.80797793898,631.896077161887,
631.984176384793,632.067923117583,632.151566794687,632.235127538841,632.318625400886,
632.402087901536,632.485533037116,632.568978872045,632.65244346737,632.735996652878,
632.819594486535,632.90332604948,632.983159886993,633.066906619599,633.150550296519,
633.234111040491,633.317608902353,633.401071402822,633.484516538222,633.567962372973,
633.65142696812,633.734980153453,633.818577986937,633.902309549713,633.982143389192,
634.065890121777,634.149533798674,634.233094542622,634.316592404458,634.4000549049,
634.48350004027,634.56694587499,634.650410470106,634.733963655405,634.817561488855,
634.901293051595,634.981126891391,635.064873624674,635.148517302272,635.232078046922,
635.315575909461,635.399038410605,635.482483546677,635.565929382098,635.649393977911,
635.732947163902,635.81654499804,635.900276561457,635.98011039359,636.063857125522,
636.147500801769,636.231061545069,636.314559406263,636.398021906071,636.481467040813,
636.564912874911,636.648377469411,636.731930654108,636.815528486962,636.899260049123,
636.979093895789,637.061786402032,637.146976686619,637.229466102182,637.311901894868,
637.394303020694,637.476688404206,637.55910075618,637.641530032067,637.724022169906,
637.743308678728),.UNSPECIFIED.);
#515=B_SPLINE_CURVE_WITH_KNOTS('',3,(#68221,#68222,#68223,#68224,#68225,
#68226,#68227,#68228,#68229,#68230,#68231,#68232,#68233,#68234,#68235,#68236,
#68237,#68238,#68239,#68240,#68241,#68242,#68243,#68244,#68245,#68246,#68247,
#68248,#68249,#68250,#68251,#68252,#68253,#68254,#68255,#68256,#68257,#68258,
#68259,#68260,#68261,#68262,#68263,#68264,#68265,#68266,#68267,#68268,#68269,
#68270,#68271,#68272,#68273,#68274,#68275,#68276,#68277,#68278,#68279,#68280,
#68281,#68282,#68283,#68284,#68285,#68286,#68287,#68288,#68289,#68290,#68291,
#68292,#68293,#68294,#68295,#68296,#68297,#68298,#68299,#68300,#68301,#68302,
#68303,#68304,#68305,#68306,#68307,#68308,#68309,#68310,#68311,#68312,#68313,
#68314,#68315,#68316,#68317,#68318,#68319,#68320,#68321,#68322,#68323,#68324,
#68325,#68326,#68327,#68328,#68329,#68330,#68331,#68332,#68333,#68334,#68335,
#68336,#68337,#68338,#68339,#68340,#68341,#68342,#68343,#68344,#68345,#68346,
#68347,#68348,#68349,#68350,#68351,#68352,#68353,#68354,#68355,#68356,#68357,
#68358,#68359,#68360,#68361,#68362,#68363,#68364,#68365,#68366,#68367,#68368,
#68369,#68370,#68371,#68372,#68373,#68374,#68375,#68376,#68377,#68378,#68379,
#68380,#68381,#68382,#68383,#68384,#68385,#68386,#68387,#68388,#68389,#68390,
#68391,#68392,#68393,#68394,#68395,#68396,#68397,#68398,#68399,#68400,#68401,
#68402,#68403,#68404,#68405,#68406,#68407,#68408,#68409,#68410,#68411,#68412,
#68413,#68414,#68415,#68416,#68417,#68418,#68419,#68420,#68421,#68422,#68423,
#68424,#68425,#68426,#68427,#68428,#68429,#68430,#68431,#68432,#68433,#68434,
#68435,#68436,#68437,#68438,#68439,#68440,#68441,#68442,#68443,#68444,#68445,
#68446,#68447,#68448,#68449),.UNSPECIFIED.,.F.,.F.,(4,3,3,3,3,3,3,3,3,3,
3,3,3,3,3,3,3,3,3,3,3,3,3,3,3,3,3,3,3,3,3,3,3,3,3,3,3,3,3,3,3,3,3,3,3,3,
3,3,3,3,3,3,3,3,3,3,3,3,3,3,3,3,3,3,3,3,3,3,3,3,3,3,3,3,3,3,4),(637.743308678919,
637.853102143197,637.965883558142,637.978077397988,638.061824134453,638.145467815241,
638.229028563087,638.312526428825,638.39598893316,638.479434072418,638.562879911016,
638.646344509996,638.729897699117,638.813495536373,638.89722710285,638.977060900188,
639.060807626974,639.144451298083,639.228012036256,639.311509892338,639.394972387078,
639.478417516778,639.561863345865,639.64532793539,639.728881115197,639.812478943199,
639.896210500623,639.976044402387,640.059791133763,640.143434809401,640.226995552038,
640.310493412517,640.393955911532,640.477401045437,640.560846878652,640.644311472225,
640.727864655931,640.811462487759,640.895194048843,640.975027904586,641.058774661087,
641.142418361982,641.225979129983,641.309477015903,641.392939540389,641.476384699777,
641.559830558465,641.643295177476,641.726848386422,641.810446243421,641.894177829305,
641.974011406785,642.057758095575,642.141401728705,642.224962428956,642.308460247211,
642.391922704397,642.475367796717,642.558813588631,642.642278141223,642.725831284686,
642.809429076606,642.893160598758,642.972994908984,643.056741646573,643.140385328139,
643.223946076417,643.307443942247,643.390906446161,643.474351584687,643.557797422244,
643.641262019876,643.724815207176,643.80841304235,643.892144606327,643.971978411183,
644.026493985907),.UNSPECIFIED.);
#516=B_SPLINE_CURVE_WITH_KNOTS('',3,(#68451,#68452,#68453,#68454,#68455,
#68456,#68457,#68458,#68459,#68460,#68461,#68462,#68463,#68464,#68465,#68466,
#68467,#68468,#68469,#68470,#68471,#68472,#68473,#68474,#68475,#68476,#68477,
#68478,#68479,#68480,#68481,#68482,#68483,#68484,#68485,#68486,#68487,#68488,
#68489,#68490,#68491,#68492,#68493,#68494,#68495,#68496,#68497,#68498,#68499,
#68500,#68501,#68502,#68503,#68504,#68505,#68506,#68507,#68508,#68509,#68510,
#68511,#68512,#68513,#68514,#68515,#68516,#68517,#68518,#68519,#68520,#68521,
#68522,#68523,#68524,#68525,#68526,#68527,#68528,#68529,#68530,#68531,#68532,
#68533,#68534,#68535,#68536,#68537,#68538,#68539,#68540,#68541,#68542,#68543,
#68544,#68545,#68546,#68547,#68548,#68549,#68550,#68551,#68552,#68553,#68554,
#68555,#68556,#68557,#68558,#68559,#68560,#68561,#68562,#68563,#68564,#68565,
#68566,#68567,#68568,#68569,#68570,#68571,#68572,#68573,#68574,#68575,#68576,
#68577,#68578,#68579,#68580,#68581,#68582,#68583,#68584,#68585,#68586,#68587,
#68588,#68589,#68590,#68591,#68592,#68593,#68594,#68595,#68596,#68597,#68598,
#68599,#68600,#68601,#68602,#68603,#68604,#68605,#68606,#68607,#68608,#68609,
#68610,#68611,#68612,#68613,#68614,#68615,#68616,#68617,#68618,#68619,#68620,
#68621,#68622,#68623,#68624,#68625,#68626,#68627,#68628,#68629,#68630,#68631,
#68632,#68633,#68634,#68635,#68636,#68637,#68638,#68639,#68640,#68641,#68642,
#68643,#68644,#68645,#68646,#68647,#68648,#68649,#68650,#68651,#68652,#68653,
#68654,#68655,#68656,#68657,#68658,#68659,#68660,#68661,#68662,#68663,#68664,
#68665,#68666,#68667,#68668,#68669,#68670,#68671,#68672,#68673,#68674,#68675,
#68676,#68677,#68678,#68679),.UNSPECIFIED.,.F.,.F.,(4,3,3,3,3,3,3,3,3,3,
3,3,3,3,3,3,3,3,3,3,3,3,3,3,3,3,3,3,3,3,3,3,3,3,3,3,3,3,3,3,3,3,3,3,3,3,
3,3,3,3,3,3,3,3,3,3,3,3,3,3,3,3,3,3,3,3,3,3,3,3,3,3,3,3,3,3,4),(644.026493986012,
644.109537955112,644.192482538858,644.275348512794,644.362300187868,644.44507887594,
644.527846816126,644.610622659315,644.693425058872,644.776317805284,644.859263325024,
644.942326964429,644.970961913383,645.054708329126,645.138351689163,645.221912116555,
645.305409662465,645.388871849031,645.472316671817,645.555762195533,645.639226481512,
645.722779362358,645.806376893423,645.890108160352,645.969945415582,646.053692273466,
646.137336073569,646.22089693853,646.304394919091,646.387857534394,646.471302782264,
646.554748727028,646.638213429636,646.721766717822,646.805364651814,646.889096310106,
646.968928917781,647.052676524747,647.136321080378,647.219882706454,647.303381452869,
647.386844838472,647.470290859233,647.553737578735,647.637203057182,647.720757118529,
647.804355825444,647.8880882484,647.96791241998,648.05165691988,648.135298362673,
648.218856873399,648.302352505182,648.385812788147,648.469255713997,648.552699349197,
648.636161756846,648.719712785976,648.803308476886,648.887037941935,648.966895922179,
649.050644101301,649.134289212132,649.217851376111,649.30135064278,649.38481452026,
649.468261015592,649.551708192002,649.635174109323,649.718728578814,649.80232767779,
649.886060461603,649.965879424379,650.063250642433,650.160218070957,650.256427406118,
650.309679292896),.UNSPECIFIED.);
#517=B_SPLINE_CURVE_WITH_KNOTS('',3,(#68680,#68681,#68682,#68683,#68684,
#68685,#68686,#68687,#68688,#68689,#68690,#68691,#68692,#68693,#68694,#68695,
#68696,#68697,#68698,#68699,#68700,#68701,#68702,#68703,#68704,#68705,#68706,
#68707,#68708,#68709,#68710,#68711,#68712,#68713,#68714,#68715,#68716,#68717,
#68718,#68719,#68720,#68721,#68722,#68723,#68724,#68725,#68726,#68727,#68728,
#68729,#68730,#68731,#68732,#68733,#68734,#68735,#68736,#68737,#68738,#68739,
#68740,#68741,#68742,#68743,#68744,#68745,#68746,#68747,#68748,#68749,#68750,
#68751,#68752,#68753,#68754,#68755,#68756,#68757,#68758,#68759,#68760,#68761,
#68762,#68763,#68764,#68765,#68766,#68767,#68768,#68769,#68770,#68771,#68772,
#68773,#68774,#68775,#68776,#68777,#68778,#68779,#68780,#68781,#68782,#68783,
#68784,#68785,#68786,#68787,#68788,#68789,#68790,#68791,#68792,#68793,#68794,
#68795,#68796,#68797,#68798,#68799,#68800,#68801,#68802,#68803,#68804,#68805,
#68806,#68807,#68808,#68809,#68810,#68811,#68812,#68813,#68814,#68815,#68816,
#68817,#68818,#68819,#68820,#68821,#68822,#68823,#68824,#68825,#68826,#68827,
#68828,#68829,#68830,#68831,#68832,#68833,#68834,#68835,#68836,#68837,#68838,
#68839,#68840,#68841,#68842,#68843,#68844,#68845,#68846,#68847,#68848,#68849,
#68850,#68851,#68852,#68853,#68854,#68855,#68856,#68857,#68858,#68859,#68860,
#68861,#68862,#68863,#68864,#68865,#68866,#68867,#68868,#68869,#68870,#68871,
#68872,#68873,#68874,#68875,#68876,#68877,#68878,#68879,#68880,#68881,#68882,
#68883,#68884,#68885,#68886,#68887,#68888,#68889,#68890,#68891,#68892,#68893,
#68894,#68895,#68896,#68897,#68898,#68899,#68900,#68901,#68902,#68903,#68904,
#68905,#68906,#68907,#68908),.UNSPECIFIED.,.F.,.F.,(4,3,3,3,3,3,3,3,3,3,
3,3,3,3,3,3,3,3,3,3,3,3,3,3,3,3,3,3,3,3,3,3,3,3,3,3,3,3,3,3,3,3,3,3,3,3,
3,3,3,3,3,3,3,3,3,3,3,3,3,3,3,3,3,3,3,3,3,3,3,3,3,3,3,3,3,3,4),(650.309679293087,
650.393240888994,650.476794100226,650.560356785155,650.64394680446,650.727635725486,
650.811376412273,650.895255518796,650.964862926578,651.048594280005,651.132222559778,
651.215767904574,651.299250381044,651.382697570685,651.466127442671,651.549558075561,
651.633007544585,651.716545808257,651.800128807747,651.883845835778,651.963846428777,
652.047606764442,652.131263971344,652.214838159334,652.298349366392,652.381825016557,
652.465283180996,652.548741912418,652.63221926006,652.715784899703,652.799395044793,
652.883138552625,652.962829930976,653.046603759892,653.130274747674,653.21386298612,
653.29738849552,653.380878776592,653.464351769309,653.547825511206,653.631318036458,
653.71489902901,653.798524646585,653.882283671955,653.961813433175,654.045456562427,
654.12899646569,654.21245337217,654.295847438193,654.379206565333,654.462548596396,
654.545891689939,654.629254001462,654.712706198894,654.796203587478,654.879836649319,
654.960796935374,655.044659957653,655.128419513097,655.212095608986,655.295708181083,
655.379284019893,655.462841641018,655.546399004614,655.629974066765,655.713635427877,
655.797340356763,655.881176104609,655.959780437573,656.043939027961,656.127994732299,
656.211965259881,656.295868258194,656.379720658669,656.46354316079,656.547365129084,
656.592864600267),.UNSPECIFIED.);
#518=B_SPLINE_CURVE_WITH_KNOTS('',3,(#68944,#68945,#68946,#68947,#68948,
#68949,#68950,#68951,#68952,#68953,#68954,#68955,#68956,#68957),
 .UNSPECIFIED.,.F.,.F.,(4,2,2,2,2,2,4),(9.99999997530754E-7,0.14182095517119,
0.287631757675626,0.503086521065188,0.729440907199506,0.877555757740989,
1.02857701706101),.UNSPECIFIED.);
#519=B_SPLINE_CURVE_WITH_KNOTS('',3,(#68959,#68960,#68961,#68962,#68963,
#68964,#68965,#68966,#68967,#68968,#68969,#68970,#68971,#68972,#68973,#68974,
#68975,#68976,#68977,#68978,#68979,#68980,#68981,#68982,#68983,#68984,#68985,
#68986,#68987,#68988,#68989,#68990,#68991,#68992,#68993,#68994,#68995,#68996,
#68997,#68998),.UNSPECIFIED.,.F.,.F.,(4,3,3,3,3,3,3,3,3,3,3,3,3,4),(4.93160007214672E-5,
0.0427649574919466,0.0897675869051093,0.136885129702485,0.183792086508501,
0.226860990507049,0.271471569794514,0.316625657925887,0.36158817713321,
0.405632700818853,0.446562496691295,0.493853126657646,0.540253376387635,
0.570947559363461),.UNSPECIFIED.);
#520=B_SPLINE_CURVE_WITH_KNOTS('',3,(#69000,#69001,#69002,#69003,#69004,
#69005,#69006,#69007,#69008,#69009,#69010,#69011,#69012,#69013,#69014,#69015),
 .UNSPECIFIED.,.F.,.F.,(4,3,3,3,3,4),(0.570947559371518,0.610709772227026,
0.657923274718644,0.663253192970537,0.709071515790179,0.741547465068122),
 .UNSPECIFIED.);
#521=B_SPLINE_CURVE_WITH_KNOTS('',3,(#69016,#69017,#69018,#69019,#69020,
#69021,#69022,#69023),.UNSPECIFIED.,.F.,.F.,(4,2,2,4),(9.9999998720568E-7,
0.131584807698003,0.260004416323543,0.387888081590916),.UNSPECIFIED.);
#522=B_SPLINE_CURVE_WITH_KNOTS('',3,(#69024,#69025,#69026,#69027,#69028,
#69029,#69030,#69031,#69032,#69033,#69034,#69035,#69036),.UNSPECIFIED.,
 .F.,.F.,(4,3,3,3,4),(0.,0.035677492973614,0.0785154168662275,0.121353340758841,
0.141322436288203),.UNSPECIFIED.);
#523=B_SPLINE_CURVE_WITH_KNOTS('',3,(#71664,#71665,#71666,#71667,#71668,
#71669,#71670,#71671,#71672,#71673,#71674,#71675,#71676,#71677,#71678,#71679,
#71680,#71681,#71682,#71683,#71684,#71685,#71686,#71687,#71688,#71689,#71690,
#71691,#71692,#71693,#71694,#71695,#71696,#71697,#71698,#71699,#71700,#71701,
#71702,#71703,#71704,#71705,#71706,#71707,#71708,#71709,#71710,#71711,#71712,
#71713,#71714,#71715,#71716,#71717,#71718,#71719,#71720,#71721,#71722,#71723,
#71724,#71725,#71726,#71727,#71728,#71729,#71730,#71731,#71732,#71733,#71734,
#71735,#71736,#71737,#71738,#71739,#71740,#71741,#71742,#71743,#71744,#71745,
#71746,#71747,#71748,#71749,#71750,#71751,#71752,#71753,#71754,#71755,#71756,
#71757,#71758,#71759,#71760,#71761,#71762,#71763,#71764,#71765,#71766,#71767,
#71768,#71769,#71770,#71771,#71772),.UNSPECIFIED.,.F.,.F.,(4,3,3,3,3,3,
3,3,3,3,3,3,3,3,3,3,3,3,3,3,3,3,3,3,3,3,3,3,3,3,3,3,3,3,3,3,4),(0.,0.0425921116508081,
0.091851351018792,0.141964108158449,0.191921079243666,0.218095752617461,
0.225856603980169,0.23160484665435,0.280505726837147,0.329371060234496,
0.377847157263669,0.425414716551405,0.439775785479548,0.446420638306663,
0.452418457109636,0.499737342125707,0.546051644014923,0.591938747193708,
0.610715853224386,0.643992397049059,0.655720876057318,0.663290984417249,
0.709181628316052,0.755355716299187,0.801114214970311,0.838962703861931,
0.858401290391878,0.865203582172363,0.876928203821775,0.922101076309233,
0.967129201685174,0.987605688361699,0.997059820269138,1.00412746240269,
1.04824287918054,1.09162239942997,1.13094109509738),.UNSPECIFIED.);
#524=B_SPLINE_CURVE_WITH_KNOTS('',3,(#74389,#74390,#74391,#74392,#74393,
#74394,#74395,#74396,#74397,#74398,#74399,#74400,#74401,#74402,#74403,#74404,
#74405,#74406,#74407,#74408,#74409,#74410,#74411,#74412,#74413,#74414,#74415,
#74416,#74417,#74418,#74419,#74420,#74421,#74422,#74423,#74424,#74425,#74426,
#74427,#74428,#74429,#74430,#74431,#74432,#74433,#74434,#74435,#74436,#74437,
#74438,#74439,#74440,#74441,#74442,#74443,#74444,#74445,#74446,#74447,#74448,
#74449,#74450,#74451,#74452,#74453,#74454,#74455,#74456,#74457,#74458,#74459,
#74460,#74461,#74462,#74463,#74464,#74465,#74466,#74467,#74468,#74469,#74470,
#74471,#74472,#74473,#74474,#74475,#74476,#74477,#74478,#74479,#74480,#74481,
#74482,#74483,#74484,#74485,#74486,#74487,#74488,#74489,#74490,#74491),
 .UNSPECIFIED.,.F.,.F.,(4,3,3,3,3,3,3,3,3,3,3,3,3,3,3,3,3,3,3,3,3,3,3,3,
3,3,3,3,3,3,3,3,3,3,4),(0.,0.0356758182649354,0.0785730265952882,0.121470234925641,
0.165563949885192,0.190087645004234,0.198856444779804,0.243742273156061,
0.289203976462101,0.335107841320739,0.380915801839053,0.394295401400751,
0.400490449519785,0.447465268323391,0.494416412115105,0.541058829760706,
0.557943071789862,0.602254762481671,0.609820269595172,0.65601947932705,
0.703024739023473,0.750889917889998,0.79353081291717,0.815029168382123,
0.821776719603583,0.828059272245824,0.836527523847076,0.885339424328542,
0.934151324810009,0.958199867374806,0.969807589082792,0.977523525467601,
1.02733960679315,1.07700026305144,1.12653966532838),.UNSPECIFIED.);
#533=SHAPE_REPRESENTATION_RELATIONSHIP('SRR','None',#74566,#542);
#542=ADVANCED_BREP_SHAPE_REPRESENTATION('',(#560),#74522);
#551=STYLED_ITEM('',(#74613),#560);
#560=MANIFOLD_SOLID_BREP('Body1',#4730);
#607=FACE_BOUND('',#1004,.T.);
#608=FACE_BOUND('',#1010,.T.);
#672=PLANE('',#5076);
#673=PLANE('',#5080);
#674=PLANE('',#5081);
#675=PLANE('',#5082);
#676=PLANE('',#5083);
#677=PLANE('',#5084);
#678=PLANE('',#5085);
#679=PLANE('',#5086);
#680=PLANE('',#5087);
#681=PLANE('',#5088);
#811=FACE_OUTER_BOUND('',#1001,.T.);
#812=FACE_OUTER_BOUND('',#1002,.T.);
#813=FACE_OUTER_BOUND('',#1003,.T.);
#814=FACE_OUTER_BOUND('',#1005,.T.);
#815=FACE_OUTER_BOUND('',#1006,.T.);
#816=FACE_OUTER_BOUND('',#1007,.T.);
#817=FACE_OUTER_BOUND('',#1008,.T.);
#818=FACE_OUTER_BOUND('',#1009,.T.);
#819=FACE_OUTER_BOUND('',#1011,.T.);
#820=FACE_OUTER_BOUND('',#1012,.T.);
#821=FACE_OUTER_BOUND('',#1013,.T.);
#822=FACE_OUTER_BOUND('',#1014,.T.);
#823=FACE_OUTER_BOUND('',#1015,.T.);
#824=FACE_OUTER_BOUND('',#1016,.T.);
#825=FACE_OUTER_BOUND('',#1017,.T.);
#1001=EDGE_LOOP('',(#3618,#3619,#3620,#3621,#3622,#3623,#3624,#3625,#3626,
#3627,#3628,#3629,#3630,#3631,#3632,#3633,#3634,#3635,#3636,#3637,#3638,
#3639,#3640,#3641,#3642,#3643,#3644,#3645,#3646,#3647,#3648,#3649,#3650,
#3651,#3652,#3653,#3654,#3655,#3656,#3657,#3658,#3659,#3660,#3661,#3662,
#3663,#3664,#3665,#3666,#3667,#3668,#3669,#3670,#3671,#3672,#3673,#3674,
#3675,#3676,#3677,#3678,#3679,#3680,#3681,#3682,#3683,#3684,#3685,#3686,
#3687,#3688,#3689,#3690,#3691,#3692,#3693,#3694,#3695,#3696,#3697,#3698,
#3699,#3700,#3701,#3702,#3703,#3704,#3705,#3706,#3707,#3708,#3709,#3710,
#3711,#3712,#3713,#3714,#3715,#3716,#3717,#3718,#3719,#3720,#3721,#3722,
#3723,#3724,#3725,#3726,#3727,#3728,#3729,#3730,#3731,#3732,#3733,#3734,
#3735,#3736,#3737,#3738,#3739,#3740,#3741,#3742,#3743,#3744,#3745,#3746,
#3747,#3748,#3749,#3750,#3751,#3752,#3753,#3754,#3755,#3756,#3757,#3758,
#3759,#3760,#3761,#3762,#3763,#3764,#3765,#3766,#3767,#3768,#3769,#3770,
#3771,#3772,#3773,#3774,#3775,#3776,#3777,#3778,#3779,#3780,#3781,#3782,
#3783,#3784,#3785,#3786,#3787,#3788,#3789,#3790,#3791,#3792,#3793,#3794,
#3795,#3796,#3797,#3798,#3799,#3800,#3801,#3802,#3803,#3804,#3805,#3806,
#3807,#3808,#3809,#3810,#3811,#3812,#3813,#3814,#3815,#3816,#3817,#3818,
#3819,#3820,#3821,#3822,#3823,#3824,#3825,#3826,#3827));
#1002=EDGE_LOOP('',(#3828,#3829,#3830,#3831,#3832,#3833,#3834,#3835,#3836,
#3837,#3838,#3839,#3840,#3841,#3842,#3843,#3844,#3845,#3846,#3847,#3848,
#3849,#3850,#3851,#3852,#3853,#3854,#3855,#3856,#3857,#3858,#3859,#3860,
#3861,#3862,#3863,#3864,#3865,#3866,#3867,#3868,#3869,#3870,#3871,#3872,
#3873,#3874,#3875,#3876,#3877,#3878,#3879,#3880,#3881,#3882,#3883,#3884,
#3885,#3886,#3887,#3888,#3889,#3890,#3891,#3892,#3893,#3894,#3895,#3896,
#3897,#3898,#3899,#3900,#3901,#3902,#3903,#3904,#3905,#3906,#3907,#3908,
#3909,#3910,#3911,#3912,#3913,#3914,#3915,#3916,#3917,#3918,#3919,#3920,
#3921,#3922,#3923,#3924,#3925,#3926,#3927,#3928,#3929,#3930,#3931,#3932,
#3933,#3934,#3935,#3936,#3937,#3938,#3939,#3940,#3941,#3942,#3943,#3944,
#3945,#3946,#3947,#3948,#3949,#3950,#3951,#3952,#3953,#3954,#3955,#3956,
#3957,#3958,#3959,#3960,#3961,#3962,#3963,#3964,#3965,#3966,#3967,#3968,
#3969,#3970,#3971,#3972,#3973,#3974,#3975,#3976,#3977,#3978,#3979,#3980,
#3981,#3982,#3983,#3984,#3985,#3986,#3987,#3988,#3989,#3990,#3991,#3992,
#3993,#3994,#3995,#3996,#3997,#3998,#3999,#4000,#4001,#4002,#4003,#4004,
#4005,#4006,#4007,#4008,#4009,#4010,#4011,#4012,#4013,#4014,#4015,#4016,
#4017,#4018,#4019,#4020,#4021,#4022,#4023,#4024,#4025,#4026,#4027,#4028,
#4029,#4030,#4031,#4032,#4033,#4034,#4035,#4036,#4037));
#1003=EDGE_LOOP('',(#4038));
#1004=EDGE_LOOP('',(#4039,#4040,#4041,#4042,#4043,#4044));
#1005=EDGE_LOOP('',(#4045,#4046,#4047,#4048));
#1006=EDGE_LOOP('',(#4049,#4050,#4051,#4052));
#1007=EDGE_LOOP('',(#4053,#4054,#4055,#4056));
#1008=EDGE_LOOP('',(#4057,#4058,#4059,#4060));
#1009=EDGE_LOOP('',(#4061));
#1010=EDGE_LOOP('',(#4062,#4063,#4064,#4065,#4066,#4067,#4068));
#1011=EDGE_LOOP('',(#4069,#4070,#4071,#4072));
#1012=EDGE_LOOP('',(#4073,#4074,#4075,#4076));
#1013=EDGE_LOOP('',(#4077,#4078,#4079,#4080));
#1014=EDGE_LOOP('',(#4081,#4082,#4083,#4084,#4085,#4086));
#1015=EDGE_LOOP('',(#4087,#4088,#4089,#4090,#4091,#4092,#4093,#4094,#4095,
#4096,#4097,#4098,#4099,#4100,#4101,#4102,#4103,#4104,#4105,#4106,#4107,
#4108,#4109,#4110,#4111,#4112,#4113,#4114,#4115,#4116,#4117,#4118,#4119,
#4120,#4121,#4122,#4123,#4124,#4125,#4126,#4127,#4128,#4129,#4130,#4131,
#4132,#4133,#4134,#4135,#4136,#4137,#4138,#4139,#4140,#4141,#4142,#4143,
#4144,#4145,#4146,#4147,#4148,#4149,#4150,#4151,#4152,#4153,#4154,#4155,
#4156,#4157,#4158,#4159,#4160,#4161,#4162,#4163,#4164,#4165,#4166,#4167,
#4168,#4169,#4170,#4171,#4172,#4173,#4174,#4175,#4176,#4177,#4178,#4179,
#4180,#4181,#4182,#4183,#4184,#4185,#4186,#4187,#4188,#4189,#4190,#4191,
#4192,#4193,#4194,#4195,#4196,#4197,#4198,#4199,#4200,#4201,#4202,#4203,
#4204,#4205,#4206,#4207,#4208,#4209,#4210,#4211,#4212,#4213,#4214,#4215,
#4216,#4217,#4218,#4219,#4220,#4221,#4222,#4223,#4224,#4225,#4226,#4227,
#4228,#4229,#4230,#4231,#4232,#4233,#4234,#4235,#4236,#4237,#4238,#4239,
#4240,#4241,#4242,#4243,#4244,#4245,#4246,#4247,#4248,#4249,#4250,#4251,
#4252,#4253,#4254,#4255,#4256,#4257,#4258,#4259,#4260,#4261,#4262,#4263,
#4264,#4265,#4266,#4267,#4268,#4269,#4270,#4271,#4272,#4273,#4274,#4275,
#4276,#4277,#4278,#4279,#4280,#4281,#4282,#4283,#4284,#4285,#4286,#4287,
#4288,#4289,#4290,#4291,#4292,#4293,#4294,#4295,#4296,#4297));
#1016=EDGE_LOOP('',(#4298,#4299,#4300,#4301,#4302,#4303,#4304,#4305,#4306,
#4307,#4308,#4309,#4310,#4311,#4312,#4313,#4314,#4315,#4316,#4317,#4318,
#4319,#4320,#4321,#4322,#4323,#4324,#4325,#4326,#4327,#4328,#4329,#4330,
#4331,#4332,#4333,#4334,#4335,#4336,#4337,#4338,#4339,#4340,#4341,#4342,
#4343,#4344,#4345,#4346,#4347,#4348,#4349,#4350,#4351,#4352,#4353,#4354,
#4355,#4356,#4357,#4358,#4359,#4360,#4361,#4362,#4363,#4364,#4365,#4366,
#4367,#4368,#4369,#4370,#4371,#4372,#4373,#4374,#4375,#4376,#4377,#4378,
#4379,#4380,#4381,#4382,#4383,#4384,#4385,#4386,#4387,#4388,#4389,#4390,
#4391,#4392,#4393,#4394,#4395,#4396,#4397,#4398,#4399,#4400,#4401,#4402,
#4403,#4404,#4405,#4406,#4407,#4408,#4409,#4410,#4411,#4412,#4413,#4414,
#4415,#4416,#4417,#4418,#4419,#4420,#4421,#4422,#4423,#4424,#4425,#4426,
#4427,#4428,#4429,#4430,#4431,#4432,#4433,#4434,#4435,#4436,#4437,#4438,
#4439,#4440,#4441,#4442,#4443,#4444,#4445,#4446,#4447,#4448,#4449,#4450,
#4451,#4452,#4453,#4454,#4455,#4456,#4457,#4458,#4459,#4460,#4461,#4462,
#4463,#4464,#4465,#4466,#4467,#4468,#4469,#4470,#4471,#4472,#4473,#4474,
#4475,#4476,#4477,#4478,#4479,#4480,#4481,#4482,#4483,#4484,#4485,#4486,
#4487,#4488,#4489,#4490,#4491,#4492,#4493,#4494,#4495,#4496,#4497,#4498,
#4499,#4500,#4501,#4502,#4503,#4504,#4505,#4506,#4507,#4508,#4509));
#1017=EDGE_LOOP('',(#4510,#4511,#4512,#4513));
#1196=LINE('',#68914,#1393);
#1197=LINE('',#68916,#1394);
#1198=LINE('',#68918,#1395);
#1199=LINE('',#68920,#1396);
#1200=LINE('',#68922,#1397);
#1201=LINE('',#68923,#1398);
#1202=LINE('',#68926,#1399);
#1203=LINE('',#68930,#1400);
#1204=LINE('',#68932,#1401);
#1205=LINE('',#68933,#1402);
#1206=LINE('',#68936,#1403);
#1207=LINE('',#68937,#1404);
#1208=LINE('',#68940,#1405);
#1209=LINE('',#68941,#1406);
#1210=LINE('',#69039,#1407);
#1211=LINE('',#69040,#1408);
#1212=LINE('',#69043,#1409);
#1213=LINE('',#69044,#1410);
#1214=LINE('',#69046,#1411);
#1393=VECTOR('',#5770,10.);
#1394=VECTOR('',#5771,10.);
#1395=VECTOR('',#5772,10.);
#1396=VECTOR('',#5773,10.);
#1397=VECTOR('',#5774,10.);
#1398=VECTOR('',#5775,10.);
#1399=VECTOR('',#5778,7.);
#1400=VECTOR('',#5783,10.);
#1401=VECTOR('',#5784,10.);
#1402=VECTOR('',#5785,10.);
#1403=VECTOR('',#5788,10.);
#1404=VECTOR('',#5789,10.);
#1405=VECTOR('',#5792,10.);
#1406=VECTOR('',#5793,10.);
#1407=VECTOR('',#5798,10.);
#1408=VECTOR('',#5799,10.);
#1409=VECTOR('',#5802,10.);
#1410=VECTOR('',#5803,10.);
#1411=VECTOR('',#5806,10.);
#1516=CIRCLE('',#5071,5.91675);
#1517=CIRCLE('',#5072,5.91675);
#1518=CIRCLE('',#5074,4.91825);
#1519=CIRCLE('',#5075,4.91825);
#1520=CIRCLE('',#5077,7.);
#1521=CIRCLE('',#5079,7.);
#1743=VERTEX_POINT('',#7983);
#1744=VERTEX_POINT('',#7984);
#1745=VERTEX_POINT('',#8064);
#1746=VERTEX_POINT('',#8066);
#1747=VERTEX_POINT('',#8110);
#1748=VERTEX_POINT('',#8355);
#1749=VERTEX_POINT('',#8366);
#1750=VERTEX_POINT('',#8614);
#1751=VERTEX_POINT('',#8627);
#1752=VERTEX_POINT('',#8872);
#1753=VERTEX_POINT('',#8883);
#1754=VERTEX_POINT('',#8895);
#1755=VERTEX_POINT('',#8906);
#1756=VERTEX_POINT('',#9154);
#1757=VERTEX_POINT('',#9166);
#1758=VERTEX_POINT('',#9414);
#1759=VERTEX_POINT('',#9425);
#1760=VERTEX_POINT('',#9673);
#1761=VERTEX_POINT('',#9685);
#1762=VERTEX_POINT('',#9933);
#1763=VERTEX_POINT('',#9944);
#1764=VERTEX_POINT('',#10192);
#1765=VERTEX_POINT('',#10203);
#1766=VERTEX_POINT('',#10451);
#1767=VERTEX_POINT('',#10462);
#1768=VERTEX_POINT('',#10707);
#1769=VERTEX_POINT('',#10952);
#1770=VERTEX_POINT('',#11197);
#1771=VERTEX_POINT('',#11209);
#1772=VERTEX_POINT('',#11454);
#1773=VERTEX_POINT('',#11465);
#1774=VERTEX_POINT('',#11710);
#1775=VERTEX_POINT('',#11723);
#1776=VERTEX_POINT('',#11734);
#1777=VERTEX_POINT('',#11745);
#1778=VERTEX_POINT('',#11990);
#1779=VERTEX_POINT('',#12001);
#1780=VERTEX_POINT('',#12249);
#1781=VERTEX_POINT('',#12260);
#1782=VERTEX_POINT('',#12508);
#1783=VERTEX_POINT('',#12519);
#1784=VERTEX_POINT('',#12530);
#1785=VERTEX_POINT('',#12542);
#1786=VERTEX_POINT('',#12787);
#1787=VERTEX_POINT('',#12798);
#1788=VERTEX_POINT('',#13043);
#1789=VERTEX_POINT('',#13057);
#1790=VERTEX_POINT('',#13302);
#1791=VERTEX_POINT('',#13313);
#1792=VERTEX_POINT('',#13325);
#1793=VERTEX_POINT('',#13336);
#1794=VERTEX_POINT('',#13584);
#1795=VERTEX_POINT('',#13596);
#1796=VERTEX_POINT('',#13844);
#1797=VERTEX_POINT('',#13855);
#1798=VERTEX_POINT('',#13866);
#1799=VERTEX_POINT('',#13878);
#1800=VERTEX_POINT('',#14126);
#1801=VERTEX_POINT('',#14137);
#1802=VERTEX_POINT('',#14385);
#1803=VERTEX_POINT('',#14396);
#1804=VERTEX_POINT('',#14644);
#1805=VERTEX_POINT('',#14655);
#1806=VERTEX_POINT('',#14668);
#1807=VERTEX_POINT('',#14913);
#1808=VERTEX_POINT('',#15158);
#1809=VERTEX_POINT('',#15170);
#1810=VERTEX_POINT('',#15181);
#1811=VERTEX_POINT('',#15192);
#1812=VERTEX_POINT('',#15437);
#1813=VERTEX_POINT('',#15450);
#1814=VERTEX_POINT('',#15461);
#1815=VERTEX_POINT('',#15472);
#1816=VERTEX_POINT('',#15717);
#1817=VERTEX_POINT('',#15728);
#1818=VERTEX_POINT('',#15739);
#1819=VERTEX_POINT('',#15750);
#1820=VERTEX_POINT('',#15998);
#1821=VERTEX_POINT('',#16009);
#1822=VERTEX_POINT('',#16020);
#1823=VERTEX_POINT('',#16032);
#1824=VERTEX_POINT('',#16277);
#1825=VERTEX_POINT('',#16288);
#1826=VERTEX_POINT('',#16533);
#1827=VERTEX_POINT('',#16546);
#1828=VERTEX_POINT('',#16557);
#1829=VERTEX_POINT('',#16568);
#1830=VERTEX_POINT('',#16580);
#1831=VERTEX_POINT('',#16591);
#1832=VERTEX_POINT('',#16602);
#1833=VERTEX_POINT('',#16614);
#1834=VERTEX_POINT('',#16862);
#1835=VERTEX_POINT('',#16873);
#1836=VERTEX_POINT('',#16884);
#1837=VERTEX_POINT('',#16896);
#1838=VERTEX_POINT('',#16907);
#1839=VERTEX_POINT('',#16918);
#1840=VERTEX_POINT('',#16930);
#1841=VERTEX_POINT('',#16941);
#1842=VERTEX_POINT('',#17189);
#1843=VERTEX_POINT('',#17200);
#1844=VERTEX_POINT('',#17213);
#1845=VERTEX_POINT('',#17224);
#1846=VERTEX_POINT('',#17235);
#1847=VERTEX_POINT('',#17247);
#1848=VERTEX_POINT('',#17258);
#1849=VERTEX_POINT('',#17506);
#1850=VERTEX_POINT('',#17515);
#1851=VERTEX_POINT('',#17517);
#1852=VERTEX_POINT('',#17526);
#1853=VERTEX_POINT('',#17537);
#1854=VERTEX_POINT('',#17782);
#1855=VERTEX_POINT('',#17795);
#1856=VERTEX_POINT('',#17806);
#1857=VERTEX_POINT('',#17817);
#1858=VERTEX_POINT('',#18062);
#1859=VERTEX_POINT('',#18073);
#1860=VERTEX_POINT('',#18084);
#1861=VERTEX_POINT('',#18095);
#1862=VERTEX_POINT('',#18108);
#1863=VERTEX_POINT('',#18119);
#1864=VERTEX_POINT('',#18130);
#1865=VERTEX_POINT('',#18142);
#1866=VERTEX_POINT('',#18153);
#1867=VERTEX_POINT('',#18164);
#1868=VERTEX_POINT('',#18409);
#1869=VERTEX_POINT('',#18654);
#1870=VERTEX_POINT('',#18665);
#1871=VERTEX_POINT('',#18676);
#1872=VERTEX_POINT('',#18688);
#1873=VERTEX_POINT('',#18699);
#1874=VERTEX_POINT('',#18710);
#1875=VERTEX_POINT('',#18722);
#1876=VERTEX_POINT('',#18733);
#1877=VERTEX_POINT('',#18744);
#1878=VERTEX_POINT('',#18755);
#1879=VERTEX_POINT('',#18767);
#1880=VERTEX_POINT('',#18778);
#1881=VERTEX_POINT('',#18789);
#1882=VERTEX_POINT('',#18801);
#1883=VERTEX_POINT('',#18812);
#1884=VERTEX_POINT('',#18823);
#1885=VERTEX_POINT('',#18834);
#1886=VERTEX_POINT('',#18847);
#1887=VERTEX_POINT('',#18858);
#1888=VERTEX_POINT('',#18869);
#1889=VERTEX_POINT('',#18881);
#1890=VERTEX_POINT('',#18892);
#1891=VERTEX_POINT('',#19140);
#1892=VERTEX_POINT('',#19151);
#1893=VERTEX_POINT('',#19163);
#1894=VERTEX_POINT('',#19174);
#1895=VERTEX_POINT('',#19185);
#1896=VERTEX_POINT('',#19197);
#1897=VERTEX_POINT('',#19208);
#1898=VERTEX_POINT('',#19219);
#1899=VERTEX_POINT('',#19467);
#1900=VERTEX_POINT('',#19480);
#1901=VERTEX_POINT('',#19491);
#1902=VERTEX_POINT('',#19502);
#1903=VERTEX_POINT('',#19514);
#1904=VERTEX_POINT('',#19525);
#1905=VERTEX_POINT('',#19536);
#1906=VERTEX_POINT('',#19548);
#1907=VERTEX_POINT('',#19793);
#1908=VERTEX_POINT('',#19804);
#1909=VERTEX_POINT('',#20049);
#1910=VERTEX_POINT('',#20061);
#1911=VERTEX_POINT('',#20072);
#1912=VERTEX_POINT('',#20083);
#1913=VERTEX_POINT('',#20331);
#1914=VERTEX_POINT('',#20342);
#1915=VERTEX_POINT('',#20353);
#1916=VERTEX_POINT('',#20364);
#1917=VERTEX_POINT('',#20609);
#1918=VERTEX_POINT('',#20620);
#1919=VERTEX_POINT('',#20631);
#1920=VERTEX_POINT('',#20643);
#1921=VERTEX_POINT('',#20888);
#1922=VERTEX_POINT('',#20899);
#1923=VERTEX_POINT('',#20910);
#1924=VERTEX_POINT('',#20923);
#1925=VERTEX_POINT('',#21168);
#1926=VERTEX_POINT('',#21413);
#1927=VERTEX_POINT('',#21425);
#1928=VERTEX_POINT('',#21436);
#1929=VERTEX_POINT('',#21684);
#1930=VERTEX_POINT('',#21695);
#1931=VERTEX_POINT('',#21943);
#1932=VERTEX_POINT('',#21954);
#1933=VERTEX_POINT('',#22202);
#1934=VERTEX_POINT('',#22214);
#1935=VERTEX_POINT('',#22462);
#1936=VERTEX_POINT('',#22473);
#1937=VERTEX_POINT('',#22721);
#1938=VERTEX_POINT('',#22734);
#1939=VERTEX_POINT('',#22982);
#1940=VERTEX_POINT('',#22993);
#1941=VERTEX_POINT('',#23005);
#1942=VERTEX_POINT('',#23016);
#1943=VERTEX_POINT('',#23261);
#1944=VERTEX_POINT('',#23273);
#1945=VERTEX_POINT('',#23518);
#1946=VERTEX_POINT('',#23529);
#1947=VERTEX_POINT('',#23774);
#1948=VERTEX_POINT('',#23786);
#1949=VERTEX_POINT('',#23797);
#1950=VERTEX_POINT('',#23808);
#1951=VERTEX_POINT('',#24056);
#1952=VERTEX_POINT('',#24067);
#1953=VERTEX_POINT('',#24563);
#1954=VERTEX_POINT('',#24564);
#1955=VERTEX_POINT('',#24614);
#1956=VERTEX_POINT('',#24616);
#1957=VERTEX_POINT('',#24629);
#1958=VERTEX_POINT('',#24856);
#1959=VERTEX_POINT('',#25086);
#1960=VERTEX_POINT('',#25313);
#1961=VERTEX_POINT('',#25540);
#1962=VERTEX_POINT('',#25770);
#1963=VERTEX_POINT('',#26000);
#1964=VERTEX_POINT('',#26227);
#1965=VERTEX_POINT('',#26454);
#1966=VERTEX_POINT('',#26465);
#1967=VERTEX_POINT('',#26695);
#1968=VERTEX_POINT('',#26925);
#1969=VERTEX_POINT('',#27155);
#1970=VERTEX_POINT('',#27385);
#1971=VERTEX_POINT('',#27612);
#1972=VERTEX_POINT('',#27842);
#1973=VERTEX_POINT('',#28072);
#1974=VERTEX_POINT('',#28083);
#1975=VERTEX_POINT('',#28313);
#1976=VERTEX_POINT('',#28543);
#1977=VERTEX_POINT('',#28773);
#1978=VERTEX_POINT('',#29000);
#1979=VERTEX_POINT('',#29230);
#1980=VERTEX_POINT('',#29460);
#1981=VERTEX_POINT('',#29690);
#1982=VERTEX_POINT('',#29917);
#1983=VERTEX_POINT('',#30147);
#1984=VERTEX_POINT('',#30377);
#1985=VERTEX_POINT('',#30604);
#1986=VERTEX_POINT('',#30834);
#1987=VERTEX_POINT('',#31064);
#1988=VERTEX_POINT('',#31076);
#1989=VERTEX_POINT('',#31306);
#1990=VERTEX_POINT('',#31539);
#1991=VERTEX_POINT('',#31769);
#1992=VERTEX_POINT('',#31996);
#1993=VERTEX_POINT('',#32226);
#1994=VERTEX_POINT('',#32456);
#1995=VERTEX_POINT('',#32683);
#1996=VERTEX_POINT('',#32694);
#1997=VERTEX_POINT('',#32924);
#1998=VERTEX_POINT('',#33154);
#1999=VERTEX_POINT('',#33381);
#2000=VERTEX_POINT('',#33611);
#2001=VERTEX_POINT('',#33841);
#2002=VERTEX_POINT('',#34068);
#2003=VERTEX_POINT('',#34295);
#2004=VERTEX_POINT('',#34525);
#2005=VERTEX_POINT('',#34755);
#2006=VERTEX_POINT('',#34985);
#2007=VERTEX_POINT('',#35218);
#2008=VERTEX_POINT('',#35448);
#2009=VERTEX_POINT('',#35675);
#2010=VERTEX_POINT('',#35905);
#2011=VERTEX_POINT('',#36135);
#2012=VERTEX_POINT('',#36362);
#2013=VERTEX_POINT('',#36592);
#2014=VERTEX_POINT('',#36822);
#2015=VERTEX_POINT('',#37052);
#2016=VERTEX_POINT('',#37279);
#2017=VERTEX_POINT('',#37509);
#2018=VERTEX_POINT('',#37520);
#2019=VERTEX_POINT('',#37750);
#2020=VERTEX_POINT('',#37977);
#2021=VERTEX_POINT('',#38207);
#2022=VERTEX_POINT('',#38437);
#2023=VERTEX_POINT('',#38664);
#2024=VERTEX_POINT('',#38891);
#2025=VERTEX_POINT('',#39121);
#2026=VERTEX_POINT('',#39351);
#2027=VERTEX_POINT('',#39581);
#2028=VERTEX_POINT('',#39811);
#2029=VERTEX_POINT('',#40041);
#2030=VERTEX_POINT('',#40268);
#2031=VERTEX_POINT('',#40498);
#2032=VERTEX_POINT('',#40728);
#2033=VERTEX_POINT('',#40955);
#2034=VERTEX_POINT('',#41185);
#2035=VERTEX_POINT('',#41415);
#2036=VERTEX_POINT('',#41645);
#2037=VERTEX_POINT('',#41872);
#2038=VERTEX_POINT('',#42102);
#2039=VERTEX_POINT('',#42332);
#2040=VERTEX_POINT('',#42344);
#2041=VERTEX_POINT('',#42571);
#2042=VERTEX_POINT('',#42801);
#2043=VERTEX_POINT('',#43031);
#2044=VERTEX_POINT('',#43261);
#2045=VERTEX_POINT('',#43491);
#2046=VERTEX_POINT('',#43721);
#2047=VERTEX_POINT('',#43948);
#2048=VERTEX_POINT('',#44178);
#2049=VERTEX_POINT('',#44408);
#2050=VERTEX_POINT('',#44635);
#2051=VERTEX_POINT('',#44865);
#2052=VERTEX_POINT('',#45095);
#2053=VERTEX_POINT('',#45325);
#2054=VERTEX_POINT('',#45549);
#2055=VERTEX_POINT('',#45779);
#2056=VERTEX_POINT('',#46009);
#2057=VERTEX_POINT('',#46239);
#2058=VERTEX_POINT('',#46466);
#2059=VERTEX_POINT('',#46696);
#2060=VERTEX_POINT('',#46893);
#2061=VERTEX_POINT('',#46895);
#2062=VERTEX_POINT('',#47041);
#2063=VERTEX_POINT('',#47271);
#2064=VERTEX_POINT('',#47501);
#2065=VERTEX_POINT('',#47731);
#2066=VERTEX_POINT('',#47961);
#2067=VERTEX_POINT('',#48191);
#2068=VERTEX_POINT('',#48418);
#2069=VERTEX_POINT('',#48645);
#2070=VERTEX_POINT('',#48875);
#2071=VERTEX_POINT('',#49105);
#2072=VERTEX_POINT('',#49332);
#2073=VERTEX_POINT('',#49562);
#2074=VERTEX_POINT('',#49573);
#2075=VERTEX_POINT('',#49803);
#2076=VERTEX_POINT('',#50030);
#2077=VERTEX_POINT('',#50260);
#2078=VERTEX_POINT('',#50490);
#2079=VERTEX_POINT('',#50720);
#2080=VERTEX_POINT('',#50947);
#2081=VERTEX_POINT('',#51177);
#2082=VERTEX_POINT('',#51407);
#2083=VERTEX_POINT('',#51634);
#2084=VERTEX_POINT('',#51864);
#2085=VERTEX_POINT('',#52097);
#2086=VERTEX_POINT('',#52327);
#2087=VERTEX_POINT('',#52557);
#2088=VERTEX_POINT('',#52787);
#2089=VERTEX_POINT('',#53014);
#2090=VERTEX_POINT('',#53241);
#2091=VERTEX_POINT('',#53471);
#2092=VERTEX_POINT('',#53701);
#2093=VERTEX_POINT('',#53928);
#2094=VERTEX_POINT('',#54158);
#2095=VERTEX_POINT('',#54388);
#2096=VERTEX_POINT('',#54399);
#2097=VERTEX_POINT('',#54626);
#2098=VERTEX_POINT('',#54856);
#2099=VERTEX_POINT('',#55086);
#2100=VERTEX_POINT('',#55313);
#2101=VERTEX_POINT('',#55543);
#2102=VERTEX_POINT('',#55773);
#2103=VERTEX_POINT('',#56003);
#2104=VERTEX_POINT('',#56015);
#2105=VERTEX_POINT('',#56245);
#2106=VERTEX_POINT('',#56475);
#2107=VERTEX_POINT('',#56702);
#2108=VERTEX_POINT('',#56932);
#2109=VERTEX_POINT('',#57162);
#2110=VERTEX_POINT('',#57389);
#2111=VERTEX_POINT('',#57619);
#2112=VERTEX_POINT('',#57849);
#2113=VERTEX_POINT('',#58079);
#2114=VERTEX_POINT('',#58306);
#2115=VERTEX_POINT('',#58536);
#2116=VERTEX_POINT('',#58766);
#2117=VERTEX_POINT('',#58996);
#2118=VERTEX_POINT('',#59007);
#2119=VERTEX_POINT('',#59237);
#2120=VERTEX_POINT('',#59467);
#2121=VERTEX_POINT('',#59694);
#2122=VERTEX_POINT('',#59924);
#2123=VERTEX_POINT('',#60154);
#2124=VERTEX_POINT('',#60384);
#2125=VERTEX_POINT('',#60614);
#2126=VERTEX_POINT('',#60625);
#2127=VERTEX_POINT('',#60852);
#2128=VERTEX_POINT('',#61079);
#2129=VERTEX_POINT('',#61309);
#2130=VERTEX_POINT('',#61539);
#2131=VERTEX_POINT('',#61766);
#2132=VERTEX_POINT('',#61993);
#2133=VERTEX_POINT('',#62223);
#2134=VERTEX_POINT('',#62453);
#2135=VERTEX_POINT('',#62683);
#2136=VERTEX_POINT('',#62913);
#2137=VERTEX_POINT('',#63143);
#2138=VERTEX_POINT('',#63370);
#2139=VERTEX_POINT('',#63600);
#2140=VERTEX_POINT('',#63833);
#2141=VERTEX_POINT('',#64063);
#2142=VERTEX_POINT('',#64293);
#2143=VERTEX_POINT('',#64523);
#2144=VERTEX_POINT('',#64753);
#2145=VERTEX_POINT('',#64980);
#2146=VERTEX_POINT('',#65210);
#2147=VERTEX_POINT('',#65440);
#2148=VERTEX_POINT('',#65452);
#2149=VERTEX_POINT('',#65463);
#2150=VERTEX_POINT('',#65693);
#2151=VERTEX_POINT('',#65923);
#2152=VERTEX_POINT('',#66150);
#2153=VERTEX_POINT('',#66380);
#2154=VERTEX_POINT('',#66610);
#2155=VERTEX_POINT('',#66840);
#2156=VERTEX_POINT('',#67070);
#2157=VERTEX_POINT('',#67303);
#2158=VERTEX_POINT('',#67533);
#2159=VERTEX_POINT('',#67760);
#2160=VERTEX_POINT('',#67990);
#2161=VERTEX_POINT('',#68220);
#2162=VERTEX_POINT('',#68450);
#2163=VERTEX_POINT('',#68910);
#2164=VERTEX_POINT('',#68912);
#2165=VERTEX_POINT('',#68913);
#2166=VERTEX_POINT('',#68915);
#2167=VERTEX_POINT('',#68917);
#2168=VERTEX_POINT('',#68919);
#2169=VERTEX_POINT('',#68921);
#2170=VERTEX_POINT('',#68925);
#2171=VERTEX_POINT('',#68929);
#2172=VERTEX_POINT('',#68931);
#2173=VERTEX_POINT('',#68935);
#2174=VERTEX_POINT('',#68939);
#2175=VERTEX_POINT('',#68943);
#2176=VERTEX_POINT('',#68958);
#2177=VERTEX_POINT('',#68999);
#2178=VERTEX_POINT('',#69038);
#2179=VERTEX_POINT('',#69042);
#2510=EDGE_CURVE('',#1743,#1744,#102,.T.);
#2511=EDGE_CURVE('',#1745,#1744,#1516,.F.);
#2512=EDGE_CURVE('',#1745,#1746,#103,.T.);
#2513=EDGE_CURVE('',#1746,#1747,#104,.T.);
#2514=EDGE_CURVE('',#1747,#1748,#105,.T.);
#2515=EDGE_CURVE('',#1748,#1749,#106,.T.);
#2516=EDGE_CURVE('',#1749,#1750,#107,.T.);
#2517=EDGE_CURVE('',#1750,#1751,#108,.T.);
#2518=EDGE_CURVE('',#1751,#1752,#109,.T.);
#2519=EDGE_CURVE('',#1752,#1753,#110,.T.);
#2520=EDGE_CURVE('',#1753,#1754,#111,.T.);
#2521=EDGE_CURVE('',#1754,#1755,#112,.T.);
#2522=EDGE_CURVE('',#1755,#1756,#113,.T.);
#2523=EDGE_CURVE('',#1756,#1757,#114,.T.);
#2524=EDGE_CURVE('',#1757,#1758,#115,.T.);
#2525=EDGE_CURVE('',#1758,#1759,#116,.T.);
#2526=EDGE_CURVE('',#1759,#1760,#117,.T.);
#2527=EDGE_CURVE('',#1760,#1761,#118,.T.);
#2528=EDGE_CURVE('',#1761,#1762,#119,.T.);
#2529=EDGE_CURVE('',#1762,#1763,#120,.T.);
#2530=EDGE_CURVE('',#1763,#1764,#121,.T.);
#2531=EDGE_CURVE('',#1764,#1765,#122,.T.);
#2532=EDGE_CURVE('',#1765,#1766,#123,.T.);
#2533=EDGE_CURVE('',#1766,#1767,#124,.T.);
#2534=EDGE_CURVE('',#1767,#1768,#125,.T.);
#2535=EDGE_CURVE('',#1768,#1769,#126,.T.);
#2536=EDGE_CURVE('',#1769,#1770,#127,.T.);
#2537=EDGE_CURVE('',#1770,#1771,#128,.T.);
#2538=EDGE_CURVE('',#1771,#1772,#129,.T.);
#2539=EDGE_CURVE('',#1772,#1773,#130,.T.);
#2540=EDGE_CURVE('',#1773,#1774,#131,.T.);
#2541=EDGE_CURVE('',#1774,#1775,#132,.T.);
#2542=EDGE_CURVE('',#1775,#1776,#133,.T.);
#2543=EDGE_CURVE('',#1776,#1777,#134,.T.);
#2544=EDGE_CURVE('',#1777,#1778,#135,.T.);
#2545=EDGE_CURVE('',#1778,#1779,#136,.T.);
#2546=EDGE_CURVE('',#1779,#1780,#137,.T.);
#2547=EDGE_CURVE('',#1780,#1781,#138,.T.);
#2548=EDGE_CURVE('',#1781,#1782,#139,.T.);
#2549=EDGE_CURVE('',#1782,#1783,#140,.T.);
#2550=EDGE_CURVE('',#1783,#1784,#141,.T.);
#2551=EDGE_CURVE('',#1784,#1785,#142,.T.);
#2552=EDGE_CURVE('',#1785,#1786,#143,.T.);
#2553=EDGE_CURVE('',#1786,#1787,#144,.T.);
#2554=EDGE_CURVE('',#1787,#1788,#145,.T.);
#2555=EDGE_CURVE('',#1788,#1789,#146,.T.);
#2556=EDGE_CURVE('',#1789,#1790,#147,.T.);
#2557=EDGE_CURVE('',#1790,#1791,#148,.T.);
#2558=EDGE_CURVE('',#1791,#1792,#149,.T.);
#2559=EDGE_CURVE('',#1792,#1793,#150,.T.);
#2560=EDGE_CURVE('',#1793,#1794,#151,.T.);
#2561=EDGE_CURVE('',#1794,#1795,#152,.T.);
#2562=EDGE_CURVE('',#1795,#1796,#153,.T.);
#2563=EDGE_CURVE('',#1796,#1797,#154,.T.);
#2564=EDGE_CURVE('',#1797,#1798,#155,.T.);
#2565=EDGE_CURVE('',#1798,#1799,#156,.T.);
#2566=EDGE_CURVE('',#1799,#1800,#157,.T.);
#2567=EDGE_CURVE('',#1800,#1801,#158,.T.);
#2568=EDGE_CURVE('',#1801,#1802,#159,.T.);
#2569=EDGE_CURVE('',#1802,#1803,#160,.T.);
#2570=EDGE_CURVE('',#1803,#1804,#161,.T.);
#2571=EDGE_CURVE('',#1804,#1805,#162,.T.);
#2572=EDGE_CURVE('',#1805,#1806,#163,.T.);
#2573=EDGE_CURVE('',#1806,#1807,#164,.T.);
#2574=EDGE_CURVE('',#1807,#1808,#165,.T.);
#2575=EDGE_CURVE('',#1808,#1809,#166,.T.);
#2576=EDGE_CURVE('',#1809,#1810,#167,.T.);
#2577=EDGE_CURVE('',#1810,#1811,#168,.T.);
#2578=EDGE_CURVE('',#1811,#1812,#169,.T.);
#2579=EDGE_CURVE('',#1812,#1813,#170,.T.);
#2580=EDGE_CURVE('',#1813,#1814,#171,.T.);
#2581=EDGE_CURVE('',#1814,#1815,#172,.T.);
#2582=EDGE_CURVE('',#1815,#1816,#173,.T.);
#2583=EDGE_CURVE('',#1816,#1817,#174,.T.);
#2584=EDGE_CURVE('',#1817,#1818,#175,.T.);
#2585=EDGE_CURVE('',#1818,#1819,#176,.T.);
#2586=EDGE_CURVE('',#1819,#1820,#177,.T.);
#2587=EDGE_CURVE('',#1820,#1821,#178,.T.);
#2588=EDGE_CURVE('',#1821,#1822,#179,.T.);
#2589=EDGE_CURVE('',#1822,#1823,#180,.T.);
#2590=EDGE_CURVE('',#1823,#1824,#181,.T.);
#2591=EDGE_CURVE('',#1824,#1825,#182,.T.);
#2592=EDGE_CURVE('',#1825,#1826,#183,.T.);
#2593=EDGE_CURVE('',#1826,#1827,#184,.T.);
#2594=EDGE_CURVE('',#1827,#1828,#185,.T.);
#2595=EDGE_CURVE('',#1828,#1829,#186,.T.);
#2596=EDGE_CURVE('',#1829,#1830,#187,.T.);
#2597=EDGE_CURVE('',#1830,#1831,#188,.T.);
#2598=EDGE_CURVE('',#1831,#1832,#189,.T.);
#2599=EDGE_CURVE('',#1832,#1833,#190,.T.);
#2600=EDGE_CURVE('',#1833,#1834,#191,.T.);
#2601=EDGE_CURVE('',#1834,#1835,#192,.T.);
#2602=EDGE_CURVE('',#1835,#1836,#193,.T.);
#2603=EDGE_CURVE('',#1836,#1837,#194,.T.);
#2604=EDGE_CURVE('',#1837,#1838,#195,.T.);
#2605=EDGE_CURVE('',#1838,#1839,#196,.T.);
#2606=EDGE_CURVE('',#1839,#1840,#197,.T.);
#2607=EDGE_CURVE('',#1840,#1841,#198,.T.);
#2608=EDGE_CURVE('',#1841,#1842,#199,.T.);
#2609=EDGE_CURVE('',#1842,#1843,#200,.T.);
#2610=EDGE_CURVE('',#1843,#1844,#201,.T.);
#2611=EDGE_CURVE('',#1844,#1845,#202,.T.);
#2612=EDGE_CURVE('',#1845,#1846,#203,.T.);
#2613=EDGE_CURVE('',#1846,#1847,#204,.T.);
#2614=EDGE_CURVE('',#1847,#1848,#205,.T.);
#2615=EDGE_CURVE('',#1848,#1849,#206,.T.);
#2616=EDGE_CURVE('',#1850,#1849,#1517,.T.);
#2617=EDGE_CURVE('',#1850,#1851,#207,.T.);
#2618=EDGE_CURVE('',#1851,#1852,#208,.T.);
#2619=EDGE_CURVE('',#1852,#1853,#209,.T.);
#2620=EDGE_CURVE('',#1853,#1854,#210,.T.);
#2621=EDGE_CURVE('',#1854,#1855,#211,.T.);
#2622=EDGE_CURVE('',#1855,#1856,#212,.T.);
#2623=EDGE_CURVE('',#1856,#1857,#213,.T.);
#2624=EDGE_CURVE('',#1857,#1858,#214,.T.);
#2625=EDGE_CURVE('',#1858,#1859,#215,.T.);
#2626=EDGE_CURVE('',#1859,#1860,#216,.T.);
#2627=EDGE_CURVE('',#1860,#1861,#217,.T.);
#2628=EDGE_CURVE('',#1861,#1862,#218,.T.);
#2629=EDGE_CURVE('',#1862,#1863,#219,.T.);
#2630=EDGE_CURVE('',#1863,#1864,#220,.T.);
#2631=EDGE_CURVE('',#1864,#1865,#221,.T.);
#2632=EDGE_CURVE('',#1865,#1866,#222,.T.);
#2633=EDGE_CURVE('',#1866,#1867,#223,.T.);
#2634=EDGE_CURVE('',#1867,#1868,#224,.T.);
#2635=EDGE_CURVE('',#1868,#1869,#225,.T.);
#2636=EDGE_CURVE('',#1869,#1870,#226,.T.);
#2637=EDGE_CURVE('',#1870,#1871,#227,.T.);
#2638=EDGE_CURVE('',#1871,#1872,#228,.T.);
#2639=EDGE_CURVE('',#1872,#1873,#229,.T.);
#2640=EDGE_CURVE('',#1873,#1874,#230,.T.);
#2641=EDGE_CURVE('',#1874,#1875,#231,.T.);
#2642=EDGE_CURVE('',#1875,#1876,#232,.T.);
#2643=EDGE_CURVE('',#1876,#1877,#233,.T.);
#2644=EDGE_CURVE('',#1877,#1878,#234,.T.);
#2645=EDGE_CURVE('',#1878,#1879,#235,.T.);
#2646=EDGE_CURVE('',#1879,#1880,#236,.T.);
#2647=EDGE_CURVE('',#1880,#1881,#237,.T.);
#2648=EDGE_CURVE('',#1881,#1882,#238,.T.);
#2649=EDGE_CURVE('',#1882,#1883,#239,.T.);
#2650=EDGE_CURVE('',#1883,#1884,#240,.T.);
#2651=EDGE_CURVE('',#1884,#1885,#241,.T.);
#2652=EDGE_CURVE('',#1885,#1886,#242,.T.);
#2653=EDGE_CURVE('',#1886,#1887,#243,.T.);
#2654=EDGE_CURVE('',#1887,#1888,#244,.T.);
#2655=EDGE_CURVE('',#1888,#1889,#245,.T.);
#2656=EDGE_CURVE('',#1889,#1890,#246,.T.);
#2657=EDGE_CURVE('',#1890,#1891,#247,.T.);
#2658=EDGE_CURVE('',#1891,#1892,#248,.T.);
#2659=EDGE_CURVE('',#1892,#1893,#249,.T.);
#2660=EDGE_CURVE('',#1893,#1894,#250,.T.);
#2661=EDGE_CURVE('',#1894,#1895,#251,.T.);
#2662=EDGE_CURVE('',#1895,#1896,#252,.T.);
#2663=EDGE_CURVE('',#1896,#1897,#253,.T.);
#2664=EDGE_CURVE('',#1897,#1898,#254,.T.);
#2665=EDGE_CURVE('',#1898,#1899,#255,.T.);
#2666=EDGE_CURVE('',#1899,#1900,#256,.T.);
#2667=EDGE_CURVE('',#1900,#1901,#257,.T.);
#2668=EDGE_CURVE('',#1901,#1902,#258,.T.);
#2669=EDGE_CURVE('',#1902,#1903,#259,.T.);
#2670=EDGE_CURVE('',#1903,#1904,#260,.T.);
#2671=EDGE_CURVE('',#1904,#1905,#261,.T.);
#2672=EDGE_CURVE('',#1905,#1906,#262,.T.);
#2673=EDGE_CURVE('',#1906,#1907,#263,.T.);
#2674=EDGE_CURVE('',#1907,#1908,#264,.T.);
#2675=EDGE_CURVE('',#1908,#1909,#265,.T.);
#2676=EDGE_CURVE('',#1909,#1910,#266,.T.);
#2677=EDGE_CURVE('',#1910,#1911,#267,.T.);
#2678=EDGE_CURVE('',#1911,#1912,#268,.T.);
#2679=EDGE_CURVE('',#1912,#1913,#269,.T.);
#2680=EDGE_CURVE('',#1913,#1914,#270,.T.);
#2681=EDGE_CURVE('',#1914,#1915,#271,.T.);
#2682=EDGE_CURVE('',#1915,#1916,#272,.T.);
#2683=EDGE_CURVE('',#1916,#1917,#273,.T.);
#2684=EDGE_CURVE('',#1917,#1918,#274,.T.);
#2685=EDGE_CURVE('',#1918,#1919,#275,.T.);
#2686=EDGE_CURVE('',#1919,#1920,#276,.T.);
#2687=EDGE_CURVE('',#1920,#1921,#277,.T.);
#2688=EDGE_CURVE('',#1921,#1922,#278,.T.);
#2689=EDGE_CURVE('',#1922,#1923,#279,.T.);
#2690=EDGE_CURVE('',#1923,#1924,#280,.T.);
#2691=EDGE_CURVE('',#1924,#1925,#281,.T.);
#2692=EDGE_CURVE('',#1925,#1926,#282,.T.);
#2693=EDGE_CURVE('',#1926,#1927,#283,.T.);
#2694=EDGE_CURVE('',#1927,#1928,#284,.T.);
#2695=EDGE_CURVE('',#1928,#1929,#285,.T.);
#2696=EDGE_CURVE('',#1929,#1930,#286,.T.);
#2697=EDGE_CURVE('',#1930,#1931,#287,.T.);
#2698=EDGE_CURVE('',#1931,#1932,#288,.T.);
#2699=EDGE_CURVE('',#1932,#1933,#289,.T.);
#2700=EDGE_CURVE('',#1933,#1934,#290,.T.);
#2701=EDGE_CURVE('',#1934,#1935,#291,.T.);
#2702=EDGE_CURVE('',#1935,#1936,#292,.T.);
#2703=EDGE_CURVE('',#1936,#1937,#293,.T.);
#2704=EDGE_CURVE('',#1937,#1938,#294,.T.);
#2705=EDGE_CURVE('',#1938,#1939,#295,.T.);
#2706=EDGE_CURVE('',#1939,#1940,#296,.T.);
#2707=EDGE_CURVE('',#1940,#1941,#297,.T.);
#2708=EDGE_CURVE('',#1941,#1942,#298,.T.);
#2709=EDGE_CURVE('',#1942,#1943,#299,.T.);
#2710=EDGE_CURVE('',#1943,#1944,#300,.T.);
#2711=EDGE_CURVE('',#1944,#1945,#301,.T.);
#2712=EDGE_CURVE('',#1945,#1946,#302,.T.);
#2713=EDGE_CURVE('',#1946,#1947,#303,.T.);
#2714=EDGE_CURVE('',#1947,#1948,#304,.T.);
#2715=EDGE_CURVE('',#1948,#1949,#305,.T.);
#2716=EDGE_CURVE('',#1949,#1950,#306,.T.);
#2717=EDGE_CURVE('',#1950,#1951,#307,.T.);
#2718=EDGE_CURVE('',#1951,#1952,#308,.T.);
#2719=EDGE_CURVE('',#1952,#1743,#309,.T.);
#2720=EDGE_CURVE('',#1953,#1954,#310,.T.);
#2721=EDGE_CURVE('',#1955,#1954,#1518,.T.);
#2722=EDGE_CURVE('',#1956,#1955,#311,.T.);
#2723=EDGE_CURVE('',#1957,#1956,#312,.T.);
#2724=EDGE_CURVE('',#1958,#1957,#313,.T.);
#2725=EDGE_CURVE('',#1959,#1958,#314,.T.);
#2726=EDGE_CURVE('',#1960,#1959,#315,.T.);
#2727=EDGE_CURVE('',#1961,#1960,#316,.T.);
#2728=EDGE_CURVE('',#1962,#1961,#317,.T.);
#2729=EDGE_CURVE('',#1963,#1962,#318,.T.);
#2730=EDGE_CURVE('',#1964,#1963,#319,.T.);
#2731=EDGE_CURVE('',#1965,#1964,#320,.T.);
#2732=EDGE_CURVE('',#1966,#1965,#321,.T.);
#2733=EDGE_CURVE('',#1967,#1966,#322,.T.);
#2734=EDGE_CURVE('',#1968,#1967,#323,.T.);
#2735=EDGE_CURVE('',#1969,#1968,#324,.T.);
#2736=EDGE_CURVE('',#1970,#1969,#325,.T.);
#2737=EDGE_CURVE('',#1971,#1970,#326,.T.);
#2738=EDGE_CURVE('',#1972,#1971,#327,.T.);
#2739=EDGE_CURVE('',#1973,#1972,#328,.T.);
#2740=EDGE_CURVE('',#1974,#1973,#329,.T.);
#2741=EDGE_CURVE('',#1975,#1974,#330,.T.);
#2742=EDGE_CURVE('',#1976,#1975,#331,.T.);
#2743=EDGE_CURVE('',#1977,#1976,#332,.T.);
#2744=EDGE_CURVE('',#1978,#1977,#333,.T.);
#2745=EDGE_CURVE('',#1979,#1978,#334,.T.);
#2746=EDGE_CURVE('',#1980,#1979,#335,.T.);
#2747=EDGE_CURVE('',#1981,#1980,#336,.T.);
#2748=EDGE_CURVE('',#1982,#1981,#337,.T.);
#2749=EDGE_CURVE('',#1983,#1982,#338,.T.);
#2750=EDGE_CURVE('',#1984,#1983,#339,.T.);
#2751=EDGE_CURVE('',#1985,#1984,#340,.T.);
#2752=EDGE_CURVE('',#1986,#1985,#341,.T.);
#2753=EDGE_CURVE('',#1987,#1986,#342,.T.);
#2754=EDGE_CURVE('',#1988,#1987,#343,.T.);
#2755=EDGE_CURVE('',#1989,#1988,#344,.T.);
#2756=EDGE_CURVE('',#1990,#1989,#345,.T.);
#2757=EDGE_CURVE('',#1991,#1990,#346,.T.);
#2758=EDGE_CURVE('',#1992,#1991,#347,.T.);
#2759=EDGE_CURVE('',#1993,#1992,#348,.T.);
#2760=EDGE_CURVE('',#1994,#1993,#349,.T.);
#2761=EDGE_CURVE('',#1995,#1994,#350,.T.);
#2762=EDGE_CURVE('',#1996,#1995,#351,.T.);
#2763=EDGE_CURVE('',#1997,#1996,#352,.T.);
#2764=EDGE_CURVE('',#1998,#1997,#353,.T.);
#2765=EDGE_CURVE('',#1999,#1998,#354,.T.);
#2766=EDGE_CURVE('',#2000,#1999,#355,.T.);
#2767=EDGE_CURVE('',#2001,#2000,#356,.T.);
#2768=EDGE_CURVE('',#2002,#2001,#357,.T.);
#2769=EDGE_CURVE('',#2003,#2002,#358,.T.);
#2770=EDGE_CURVE('',#2004,#2003,#359,.T.);
#2771=EDGE_CURVE('',#2005,#2004,#360,.T.);
#2772=EDGE_CURVE('',#2006,#2005,#361,.T.);
#2773=EDGE_CURVE('',#2007,#2006,#362,.T.);
#2774=EDGE_CURVE('',#2008,#2007,#363,.T.);
#2775=EDGE_CURVE('',#2009,#2008,#364,.T.);
#2776=EDGE_CURVE('',#2010,#2009,#365,.T.);
#2777=EDGE_CURVE('',#2011,#2010,#366,.T.);
#2778=EDGE_CURVE('',#2012,#2011,#367,.T.);
#2779=EDGE_CURVE('',#2013,#2012,#368,.T.);
#2780=EDGE_CURVE('',#2014,#2013,#369,.T.);
#2781=EDGE_CURVE('',#2015,#2014,#370,.T.);
#2782=EDGE_CURVE('',#2016,#2015,#371,.T.);
#2783=EDGE_CURVE('',#2017,#2016,#372,.T.);
#2784=EDGE_CURVE('',#2018,#2017,#373,.T.);
#2785=EDGE_CURVE('',#2019,#2018,#374,.T.);
#2786=EDGE_CURVE('',#2020,#2019,#375,.T.);
#2787=EDGE_CURVE('',#2021,#2020,#376,.T.);
#2788=EDGE_CURVE('',#2022,#2021,#377,.T.);
#2789=EDGE_CURVE('',#2023,#2022,#378,.T.);
#2790=EDGE_CURVE('',#2024,#2023,#379,.T.);
#2791=EDGE_CURVE('',#2025,#2024,#380,.T.);
#2792=EDGE_CURVE('',#2026,#2025,#381,.T.);
#2793=EDGE_CURVE('',#2027,#2026,#382,.T.);
#2794=EDGE_CURVE('',#2028,#2027,#383,.T.);
#2795=EDGE_CURVE('',#2029,#2028,#384,.T.);
#2796=EDGE_CURVE('',#2030,#2029,#385,.T.);
#2797=EDGE_CURVE('',#2031,#2030,#386,.T.);
#2798=EDGE_CURVE('',#2032,#2031,#387,.T.);
#2799=EDGE_CURVE('',#2033,#2032,#388,.T.);
#2800=EDGE_CURVE('',#2034,#2033,#389,.T.);
#2801=EDGE_CURVE('',#2035,#2034,#390,.T.);
#2802=EDGE_CURVE('',#2036,#2035,#391,.T.);
#2803=EDGE_CURVE('',#2037,#2036,#392,.T.);
#2804=EDGE_CURVE('',#2038,#2037,#393,.T.);
#2805=EDGE_CURVE('',#2039,#2038,#394,.T.);
#2806=EDGE_CURVE('',#2040,#2039,#395,.T.);
#2807=EDGE_CURVE('',#2041,#2040,#396,.T.);
#2808=EDGE_CURVE('',#2042,#2041,#397,.T.);
#2809=EDGE_CURVE('',#2043,#2042,#398,.T.);
#2810=EDGE_CURVE('',#2044,#2043,#399,.T.);
#2811=EDGE_CURVE('',#2045,#2044,#400,.T.);
#2812=EDGE_CURVE('',#2046,#2045,#401,.T.);
#2813=EDGE_CURVE('',#2047,#2046,#402,.T.);
#2814=EDGE_CURVE('',#2048,#2047,#403,.T.);
#2815=EDGE_CURVE('',#2049,#2048,#404,.T.);
#2816=EDGE_CURVE('',#2050,#2049,#405,.T.);
#2817=EDGE_CURVE('',#2051,#2050,#406,.T.);
#2818=EDGE_CURVE('',#2052,#2051,#407,.T.);
#2819=EDGE_CURVE('',#2053,#2052,#408,.T.);
#2820=EDGE_CURVE('',#2054,#2053,#409,.T.);
#2821=EDGE_CURVE('',#2055,#2054,#410,.T.);
#2822=EDGE_CURVE('',#2056,#2055,#411,.T.);
#2823=EDGE_CURVE('',#2057,#2056,#412,.T.);
#2824=EDGE_CURVE('',#2058,#2057,#413,.T.);
#2825=EDGE_CURVE('',#2059,#2058,#414,.T.);
#2826=EDGE_CURVE('',#2060,#2059,#1519,.T.);
#2827=EDGE_CURVE('',#2060,#2061,#415,.T.);
#2828=EDGE_CURVE('',#2061,#2062,#416,.T.);
#2829=EDGE_CURVE('',#2062,#2063,#417,.T.);
#2830=EDGE_CURVE('',#2063,#2064,#418,.T.);
#2831=EDGE_CURVE('',#2064,#2065,#419,.T.);
#2832=EDGE_CURVE('',#2065,#2066,#420,.T.);
#2833=EDGE_CURVE('',#2066,#2067,#421,.T.);
#2834=EDGE_CURVE('',#2067,#2068,#422,.T.);
#2835=EDGE_CURVE('',#2068,#2069,#423,.T.);
#2836=EDGE_CURVE('',#2069,#2070,#424,.T.);
#2837=EDGE_CURVE('',#2070,#2071,#425,.T.);
#2838=EDGE_CURVE('',#2071,#2072,#426,.T.);
#2839=EDGE_CURVE('',#2072,#2073,#427,.T.);
#2840=EDGE_CURVE('',#2073,#2074,#428,.T.);
#2841=EDGE_CURVE('',#2074,#2075,#429,.T.);
#2842=EDGE_CURVE('',#2075,#2076,#430,.T.);
#2843=EDGE_CURVE('',#2076,#2077,#431,.T.);
#2844=EDGE_CURVE('',#2077,#2078,#432,.T.);
#2845=EDGE_CURVE('',#2078,#2079,#433,.T.);
#2846=EDGE_CURVE('',#2079,#2080,#434,.T.);
#2847=EDGE_CURVE('',#2080,#2081,#435,.T.);
#2848=EDGE_CURVE('',#2081,#2082,#436,.T.);
#2849=EDGE_CURVE('',#2082,#2083,#437,.T.);
#2850=EDGE_CURVE('',#2083,#2084,#438,.T.);
#2851=EDGE_CURVE('',#2084,#2085,#439,.T.);
#2852=EDGE_CURVE('',#2085,#2086,#440,.T.);
#2853=EDGE_CURVE('',#2086,#2087,#441,.T.);
#2854=EDGE_CURVE('',#2087,#2088,#442,.T.);
#2855=EDGE_CURVE('',#2088,#2089,#443,.T.);
#2856=EDGE_CURVE('',#2089,#2090,#444,.T.);
#2857=EDGE_CURVE('',#2090,#2091,#445,.T.);
#2858=EDGE_CURVE('',#2091,#2092,#446,.T.);
#2859=EDGE_CURVE('',#2092,#2093,#447,.T.);
#2860=EDGE_CURVE('',#2093,#2094,#448,.T.);
#2861=EDGE_CURVE('',#2094,#2095,#449,.T.);
#2862=EDGE_CURVE('',#2095,#2096,#450,.T.);
#2863=EDGE_CURVE('',#2096,#2097,#451,.T.);
#2864=EDGE_CURVE('',#2097,#2098,#452,.T.);
#2865=EDGE_CURVE('',#2098,#2099,#453,.T.);
#2866=EDGE_CURVE('',#2099,#2100,#454,.T.);
#2867=EDGE_CURVE('',#2100,#2101,#455,.T.);
#2868=EDGE_CURVE('',#2101,#2102,#456,.T.);
#2869=EDGE_CURVE('',#2102,#2103,#457,.T.);
#2870=EDGE_CURVE('',#2103,#2104,#458,.T.);
#2871=EDGE_CURVE('',#2104,#2105,#459,.T.);
#2872=EDGE_CURVE('',#2105,#2106,#460,.T.);
#2873=EDGE_CURVE('',#2106,#2107,#461,.T.);
#2874=EDGE_CURVE('',#2107,#2108,#462,.T.);
#2875=EDGE_CURVE('',#2108,#2109,#463,.T.);
#2876=EDGE_CURVE('',#2109,#2110,#464,.T.);
#2877=EDGE_CURVE('',#2110,#2111,#465,.T.);
#2878=EDGE_CURVE('',#2111,#2112,#466,.T.);
#2879=EDGE_CURVE('',#2112,#2113,#467,.T.);
#2880=EDGE_CURVE('',#2113,#2114,#468,.T.);
#2881=EDGE_CURVE('',#2114,#2115,#469,.T.);
#2882=EDGE_CURVE('',#2115,#2116,#470,.T.);
#2883=EDGE_CURVE('',#2116,#2117,#471,.T.);
#2884=EDGE_CURVE('',#2117,#2118,#472,.T.);
#2885=EDGE_CURVE('',#2118,#2119,#473,.T.);
#2886=EDGE_CURVE('',#2119,#2120,#474,.T.);
#2887=EDGE_CURVE('',#2120,#2121,#475,.T.);
#2888=EDGE_CURVE('',#2121,#2122,#476,.T.);
#2889=EDGE_CURVE('',#2122,#2123,#477,.T.);
#2890=EDGE_CURVE('',#2123,#2124,#478,.T.);
#2891=EDGE_CURVE('',#2124,#2125,#479,.T.);
#2892=EDGE_CURVE('',#2125,#2126,#480,.T.);
#2893=EDGE_CURVE('',#2126,#2127,#481,.T.);
#2894=EDGE_CURVE('',#2127,#2128,#482,.T.);
#2895=EDGE_CURVE('',#2128,#2129,#483,.T.);
#2896=EDGE_CURVE('',#2129,#2130,#484,.T.);
#2897=EDGE_CURVE('',#2130,#2131,#485,.T.);
#2898=EDGE_CURVE('',#2131,#2132,#486,.T.);
#2899=EDGE_CURVE('',#2132,#2133,#487,.T.);
#2900=EDGE_CURVE('',#2133,#2134,#488,.T.);
#2901=EDGE_CURVE('',#2134,#2135,#489,.T.);
#2902=EDGE_CURVE('',#2135,#2136,#490,.T.);
#2903=EDGE_CURVE('',#2136,#2137,#491,.T.);
#2904=EDGE_CURVE('',#2137,#2138,#492,.T.);
#2905=EDGE_CURVE('',#2138,#2139,#493,.T.);
#2906=EDGE_CURVE('',#2139,#2140,#494,.T.);
#2907=EDGE_CURVE('',#2140,#2141,#495,.T.);
#2908=EDGE_CURVE('',#2141,#2142,#496,.T.);
#2909=EDGE_CURVE('',#2142,#2143,#497,.T.);
#2910=EDGE_CURVE('',#2143,#2144,#498,.T.);
#2911=EDGE_CURVE('',#2144,#2145,#499,.T.);
#2912=EDGE_CURVE('',#2145,#2146,#500,.T.);
#2913=EDGE_CURVE('',#2146,#2147,#501,.T.);
#2914=EDGE_CURVE('',#2147,#2148,#502,.T.);
#2915=EDGE_CURVE('',#2148,#2149,#503,.T.);
#2916=EDGE_CURVE('',#2149,#2150,#504,.T.);
#2917=EDGE_CURVE('',#2150,#2151,#505,.T.);
#2918=EDGE_CURVE('',#2151,#2152,#506,.T.);
#2919=EDGE_CURVE('',#2152,#2153,#507,.T.);
#2920=EDGE_CURVE('',#2153,#2154,#508,.T.);
#2921=EDGE_CURVE('',#2154,#2155,#509,.T.);
#2922=EDGE_CURVE('',#2155,#2156,#510,.T.);
#2923=EDGE_CURVE('',#2156,#2157,#511,.T.);
#2924=EDGE_CURVE('',#2157,#2158,#512,.T.);
#2925=EDGE_CURVE('',#2158,#2159,#513,.T.);
#2926=EDGE_CURVE('',#2159,#2160,#514,.T.);
#2927=EDGE_CURVE('',#2160,#2161,#515,.T.);
#2928=EDGE_CURVE('',#2161,#2162,#516,.T.);
#2929=EDGE_CURVE('',#2162,#1953,#517,.T.);
#2930=EDGE_CURVE('',#2163,#2163,#1520,.T.);
#2931=EDGE_CURVE('',#2164,#2165,#1196,.T.);
#2932=EDGE_CURVE('',#2166,#2164,#1197,.T.);
#2933=EDGE_CURVE('',#2167,#2166,#1198,.T.);
#2934=EDGE_CURVE('',#2168,#2167,#1199,.T.);
#2935=EDGE_CURVE('',#2169,#2168,#1200,.T.);
#2936=EDGE_CURVE('',#2165,#2169,#1201,.T.);
#2937=EDGE_CURVE('',#2163,#2170,#1202,.T.);
#2938=EDGE_CURVE('',#2170,#2170,#1521,.T.);
#2939=EDGE_CURVE('',#2167,#2171,#1203,.T.);
#2940=EDGE_CURVE('',#2172,#2171,#1204,.T.);
#2941=EDGE_CURVE('',#2168,#2172,#1205,.T.);
#2942=EDGE_CURVE('',#2166,#2173,#1206,.T.);
#2943=EDGE_CURVE('',#2171,#2173,#1207,.T.);
#2944=EDGE_CURVE('',#2164,#2174,#1208,.T.);
#2945=EDGE_CURVE('',#2173,#2174,#1209,.T.);
#2946=EDGE_CURVE('',#2175,#1745,#518,.T.);
#2947=EDGE_CURVE('',#1744,#2176,#519,.T.);
#2948=EDGE_CURVE('',#2176,#2177,#520,.T.);
#2949=EDGE_CURVE('',#2177,#2060,#521,.T.);
#2950=EDGE_CURVE('',#2059,#2175,#522,.T.);
#2951=EDGE_CURVE('',#2165,#2178,#1210,.T.);
#2952=EDGE_CURVE('',#2174,#2178,#1211,.T.);
#2953=EDGE_CURVE('',#2179,#2172,#1212,.T.);
#2954=EDGE_CURVE('',#2169,#2179,#1213,.T.);
#2955=EDGE_CURVE('',#2178,#2179,#1214,.T.);
#2956=EDGE_CURVE('',#1849,#1955,#523,.T.);
#2957=EDGE_CURVE('',#1954,#1850,#524,.T.);
#3618=ORIENTED_EDGE('',*,*,#2510,.T.);
#3619=ORIENTED_EDGE('',*,*,#2511,.F.);
#3620=ORIENTED_EDGE('',*,*,#2512,.T.);
#3621=ORIENTED_EDGE('',*,*,#2513,.T.);
#3622=ORIENTED_EDGE('',*,*,#2514,.T.);
#3623=ORIENTED_EDGE('',*,*,#2515,.T.);
#3624=ORIENTED_EDGE('',*,*,#2516,.T.);
#3625=ORIENTED_EDGE('',*,*,#2517,.T.);
#3626=ORIENTED_EDGE('',*,*,#2518,.T.);
#3627=ORIENTED_EDGE('',*,*,#2519,.T.);
#3628=ORIENTED_EDGE('',*,*,#2520,.T.);
#3629=ORIENTED_EDGE('',*,*,#2521,.T.);
#3630=ORIENTED_EDGE('',*,*,#2522,.T.);
#3631=ORIENTED_EDGE('',*,*,#2523,.T.);
#3632=ORIENTED_EDGE('',*,*,#2524,.T.);
#3633=ORIENTED_EDGE('',*,*,#2525,.T.);
#3634=ORIENTED_EDGE('',*,*,#2526,.T.);
#3635=ORIENTED_EDGE('',*,*,#2527,.T.);
#3636=ORIENTED_EDGE('',*,*,#2528,.T.);
#3637=ORIENTED_EDGE('',*,*,#2529,.T.);
#3638=ORIENTED_EDGE('',*,*,#2530,.T.);
#3639=ORIENTED_EDGE('',*,*,#2531,.T.);
#3640=ORIENTED_EDGE('',*,*,#2532,.T.);
#3641=ORIENTED_EDGE('',*,*,#2533,.T.);
#3642=ORIENTED_EDGE('',*,*,#2534,.T.);
#3643=ORIENTED_EDGE('',*,*,#2535,.T.);
#3644=ORIENTED_EDGE('',*,*,#2536,.T.);
#3645=ORIENTED_EDGE('',*,*,#2537,.T.);
#3646=ORIENTED_EDGE('',*,*,#2538,.T.);
#3647=ORIENTED_EDGE('',*,*,#2539,.T.);
#3648=ORIENTED_EDGE('',*,*,#2540,.T.);
#3649=ORIENTED_EDGE('',*,*,#2541,.T.);
#3650=ORIENTED_EDGE('',*,*,#2542,.T.);
#3651=ORIENTED_EDGE('',*,*,#2543,.T.);
#3652=ORIENTED_EDGE('',*,*,#2544,.T.);
#3653=ORIENTED_EDGE('',*,*,#2545,.T.);
#3654=ORIENTED_EDGE('',*,*,#2546,.T.);
#3655=ORIENTED_EDGE('',*,*,#2547,.T.);
#3656=ORIENTED_EDGE('',*,*,#2548,.T.);
#3657=ORIENTED_EDGE('',*,*,#2549,.T.);
#3658=ORIENTED_EDGE('',*,*,#2550,.T.);
#3659=ORIENTED_EDGE('',*,*,#2551,.T.);
#3660=ORIENTED_EDGE('',*,*,#2552,.T.);
#3661=ORIENTED_EDGE('',*,*,#2553,.T.);
#3662=ORIENTED_EDGE('',*,*,#2554,.T.);
#3663=ORIENTED_EDGE('',*,*,#2555,.T.);
#3664=ORIENTED_EDGE('',*,*,#2556,.T.);
#3665=ORIENTED_EDGE('',*,*,#2557,.T.);
#3666=ORIENTED_EDGE('',*,*,#2558,.T.);
#3667=ORIENTED_EDGE('',*,*,#2559,.T.);
#3668=ORIENTED_EDGE('',*,*,#2560,.T.);
#3669=ORIENTED_EDGE('',*,*,#2561,.T.);
#3670=ORIENTED_EDGE('',*,*,#2562,.T.);
#3671=ORIENTED_EDGE('',*,*,#2563,.T.);
#3672=ORIENTED_EDGE('',*,*,#2564,.T.);
#3673=ORIENTED_EDGE('',*,*,#2565,.T.);
#3674=ORIENTED_EDGE('',*,*,#2566,.T.);
#3675=ORIENTED_EDGE('',*,*,#2567,.T.);
#3676=ORIENTED_EDGE('',*,*,#2568,.T.);
#3677=ORIENTED_EDGE('',*,*,#2569,.T.);
#3678=ORIENTED_EDGE('',*,*,#2570,.T.);
#3679=ORIENTED_EDGE('',*,*,#2571,.T.);
#3680=ORIENTED_EDGE('',*,*,#2572,.T.);
#3681=ORIENTED_EDGE('',*,*,#2573,.T.);
#3682=ORIENTED_EDGE('',*,*,#2574,.T.);
#3683=ORIENTED_EDGE('',*,*,#2575,.T.);
#3684=ORIENTED_EDGE('',*,*,#2576,.T.);
#3685=ORIENTED_EDGE('',*,*,#2577,.T.);
#3686=ORIENTED_EDGE('',*,*,#2578,.T.);
#3687=ORIENTED_EDGE('',*,*,#2579,.T.);
#3688=ORIENTED_EDGE('',*,*,#2580,.T.);
#3689=ORIENTED_EDGE('',*,*,#2581,.T.);
#3690=ORIENTED_EDGE('',*,*,#2582,.T.);
#3691=ORIENTED_EDGE('',*,*,#2583,.T.);
#3692=ORIENTED_EDGE('',*,*,#2584,.T.);
#3693=ORIENTED_EDGE('',*,*,#2585,.T.);
#3694=ORIENTED_EDGE('',*,*,#2586,.T.);
#3695=ORIENTED_EDGE('',*,*,#2587,.T.);
#3696=ORIENTED_EDGE('',*,*,#2588,.T.);
#3697=ORIENTED_EDGE('',*,*,#2589,.T.);
#3698=ORIENTED_EDGE('',*,*,#2590,.T.);
#3699=ORIENTED_EDGE('',*,*,#2591,.T.);
#3700=ORIENTED_EDGE('',*,*,#2592,.T.);
#3701=ORIENTED_EDGE('',*,*,#2593,.T.);
#3702=ORIENTED_EDGE('',*,*,#2594,.T.);
#3703=ORIENTED_EDGE('',*,*,#2595,.T.);
#3704=ORIENTED_EDGE('',*,*,#2596,.T.);
#3705=ORIENTED_EDGE('',*,*,#2597,.T.);
#3706=ORIENTED_EDGE('',*,*,#2598,.T.);
#3707=ORIENTED_EDGE('',*,*,#2599,.T.);
#3708=ORIENTED_EDGE('',*,*,#2600,.T.);
#3709=ORIENTED_EDGE('',*,*,#2601,.T.);
#3710=ORIENTED_EDGE('',*,*,#2602,.T.);
#3711=ORIENTED_EDGE('',*,*,#2603,.T.);
#3712=ORIENTED_EDGE('',*,*,#2604,.T.);
#3713=ORIENTED_EDGE('',*,*,#2605,.T.);
#3714=ORIENTED_EDGE('',*,*,#2606,.T.);
#3715=ORIENTED_EDGE('',*,*,#2607,.T.);
#3716=ORIENTED_EDGE('',*,*,#2608,.T.);
#3717=ORIENTED_EDGE('',*,*,#2609,.T.);
#3718=ORIENTED_EDGE('',*,*,#2610,.T.);
#3719=ORIENTED_EDGE('',*,*,#2611,.T.);
#3720=ORIENTED_EDGE('',*,*,#2612,.T.);
#3721=ORIENTED_EDGE('',*,*,#2613,.T.);
#3722=ORIENTED_EDGE('',*,*,#2614,.T.);
#3723=ORIENTED_EDGE('',*,*,#2615,.T.);
#3724=ORIENTED_EDGE('',*,*,#2616,.F.);
#3725=ORIENTED_EDGE('',*,*,#2617,.T.);
#3726=ORIENTED_EDGE('',*,*,#2618,.T.);
#3727=ORIENTED_EDGE('',*,*,#2619,.T.);
#3728=ORIENTED_EDGE('',*,*,#2620,.T.);
#3729=ORIENTED_EDGE('',*,*,#2621,.T.);
#3730=ORIENTED_EDGE('',*,*,#2622,.T.);
#3731=ORIENTED_EDGE('',*,*,#2623,.T.);
#3732=ORIENTED_EDGE('',*,*,#2624,.T.);
#3733=ORIENTED_EDGE('',*,*,#2625,.T.);
#3734=ORIENTED_EDGE('',*,*,#2626,.T.);
#3735=ORIENTED_EDGE('',*,*,#2627,.T.);
#3736=ORIENTED_EDGE('',*,*,#2628,.T.);
#3737=ORIENTED_EDGE('',*,*,#2629,.T.);
#3738=ORIENTED_EDGE('',*,*,#2630,.T.);
#3739=ORIENTED_EDGE('',*,*,#2631,.T.);
#3740=ORIENTED_EDGE('',*,*,#2632,.T.);
#3741=ORIENTED_EDGE('',*,*,#2633,.T.);
#3742=ORIENTED_EDGE('',*,*,#2634,.T.);
#3743=ORIENTED_EDGE('',*,*,#2635,.T.);
#3744=ORIENTED_EDGE('',*,*,#2636,.T.);
#3745=ORIENTED_EDGE('',*,*,#2637,.T.);
#3746=ORIENTED_EDGE('',*,*,#2638,.T.);
#3747=ORIENTED_EDGE('',*,*,#2639,.T.);
#3748=ORIENTED_EDGE('',*,*,#2640,.T.);
#3749=ORIENTED_EDGE('',*,*,#2641,.T.);
#3750=ORIENTED_EDGE('',*,*,#2642,.T.);
#3751=ORIENTED_EDGE('',*,*,#2643,.T.);
#3752=ORIENTED_EDGE('',*,*,#2644,.T.);
#3753=ORIENTED_EDGE('',*,*,#2645,.T.);
#3754=ORIENTED_EDGE('',*,*,#2646,.T.);
#3755=ORIENTED_EDGE('',*,*,#2647,.T.);
#3756=ORIENTED_EDGE('',*,*,#2648,.T.);
#3757=ORIENTED_EDGE('',*,*,#2649,.T.);
#3758=ORIENTED_EDGE('',*,*,#2650,.T.);
#3759=ORIENTED_EDGE('',*,*,#2651,.T.);
#3760=ORIENTED_EDGE('',*,*,#2652,.T.);
#3761=ORIENTED_EDGE('',*,*,#2653,.T.);
#3762=ORIENTED_EDGE('',*,*,#2654,.T.);
#3763=ORIENTED_EDGE('',*,*,#2655,.T.);
#3764=ORIENTED_EDGE('',*,*,#2656,.T.);
#3765=ORIENTED_EDGE('',*,*,#2657,.T.);
#3766=ORIENTED_EDGE('',*,*,#2658,.T.);
#3767=ORIENTED_EDGE('',*,*,#2659,.T.);
#3768=ORIENTED_EDGE('',*,*,#2660,.T.);
#3769=ORIENTED_EDGE('',*,*,#2661,.T.);
#3770=ORIENTED_EDGE('',*,*,#2662,.T.);
#3771=ORIENTED_EDGE('',*,*,#2663,.T.);
#3772=ORIENTED_EDGE('',*,*,#2664,.T.);
#3773=ORIENTED_EDGE('',*,*,#2665,.T.);
#3774=ORIENTED_EDGE('',*,*,#2666,.T.);
#3775=ORIENTED_EDGE('',*,*,#2667,.T.);
#3776=ORIENTED_EDGE('',*,*,#2668,.T.);
#3777=ORIENTED_EDGE('',*,*,#2669,.T.);
#3778=ORIENTED_EDGE('',*,*,#2670,.T.);
#3779=ORIENTED_EDGE('',*,*,#2671,.T.);
#3780=ORIENTED_EDGE('',*,*,#2672,.T.);
#3781=ORIENTED_EDGE('',*,*,#2673,.T.);
#3782=ORIENTED_EDGE('',*,*,#2674,.T.);
#3783=ORIENTED_EDGE('',*,*,#2675,.T.);
#3784=ORIENTED_EDGE('',*,*,#2676,.T.);
#3785=ORIENTED_EDGE('',*,*,#2677,.T.);
#3786=ORIENTED_EDGE('',*,*,#2678,.T.);
#3787=ORIENTED_EDGE('',*,*,#2679,.T.);
#3788=ORIENTED_EDGE('',*,*,#2680,.T.);
#3789=ORIENTED_EDGE('',*,*,#2681,.T.);
#3790=ORIENTED_EDGE('',*,*,#2682,.T.);
#3791=ORIENTED_EDGE('',*,*,#2683,.T.);
#3792=ORIENTED_EDGE('',*,*,#2684,.T.);
#3793=ORIENTED_EDGE('',*,*,#2685,.T.);
#3794=ORIENTED_EDGE('',*,*,#2686,.T.);
#3795=ORIENTED_EDGE('',*,*,#2687,.T.);
#3796=ORIENTED_EDGE('',*,*,#2688,.T.);
#3797=ORIENTED_EDGE('',*,*,#2689,.T.);
#3798=ORIENTED_EDGE('',*,*,#2690,.T.);
#3799=ORIENTED_EDGE('',*,*,#2691,.T.);
#3800=ORIENTED_EDGE('',*,*,#2692,.T.);
#3801=ORIENTED_EDGE('',*,*,#2693,.T.);
#3802=ORIENTED_EDGE('',*,*,#2694,.T.);
#3803=ORIENTED_EDGE('',*,*,#2695,.T.);
#3804=ORIENTED_EDGE('',*,*,#2696,.T.);
#3805=ORIENTED_EDGE('',*,*,#2697,.T.);
#3806=ORIENTED_EDGE('',*,*,#2698,.T.);
#3807=ORIENTED_EDGE('',*,*,#2699,.T.);
#3808=ORIENTED_EDGE('',*,*,#2700,.T.);
#3809=ORIENTED_EDGE('',*,*,#2701,.T.);
#3810=ORIENTED_EDGE('',*,*,#2702,.T.);
#3811=ORIENTED_EDGE('',*,*,#2703,.T.);
#3812=ORIENTED_EDGE('',*,*,#2704,.T.);
#3813=ORIENTED_EDGE('',*,*,#2705,.T.);
#3814=ORIENTED_EDGE('',*,*,#2706,.T.);
#3815=ORIENTED_EDGE('',*,*,#2707,.T.);
#3816=ORIENTED_EDGE('',*,*,#2708,.T.);
#3817=ORIENTED_EDGE('',*,*,#2709,.T.);
#3818=ORIENTED_EDGE('',*,*,#2710,.T.);
#3819=ORIENTED_EDGE('',*,*,#2711,.T.);
#3820=ORIENTED_EDGE('',*,*,#2712,.T.);
#3821=ORIENTED_EDGE('',*,*,#2713,.T.);
#3822=ORIENTED_EDGE('',*,*,#2714,.T.);
#3823=ORIENTED_EDGE('',*,*,#2715,.T.);
#3824=ORIENTED_EDGE('',*,*,#2716,.T.);
#3825=ORIENTED_EDGE('',*,*,#2717,.T.);
#3826=ORIENTED_EDGE('',*,*,#2718,.T.);
#3827=ORIENTED_EDGE('',*,*,#2719,.T.);
#3828=ORIENTED_EDGE('',*,*,#2720,.T.);
#3829=ORIENTED_EDGE('',*,*,#2721,.F.);
#3830=ORIENTED_EDGE('',*,*,#2722,.F.);
#3831=ORIENTED_EDGE('',*,*,#2723,.F.);
#3832=ORIENTED_EDGE('',*,*,#2724,.F.);
#3833=ORIENTED_EDGE('',*,*,#2725,.F.);
#3834=ORIENTED_EDGE('',*,*,#2726,.F.);
#3835=ORIENTED_EDGE('',*,*,#2727,.F.);
#3836=ORIENTED_EDGE('',*,*,#2728,.F.);
#3837=ORIENTED_EDGE('',*,*,#2729,.F.);
#3838=ORIENTED_EDGE('',*,*,#2730,.F.);
#3839=ORIENTED_EDGE('',*,*,#2731,.F.);
#3840=ORIENTED_EDGE('',*,*,#2732,.F.);
#3841=ORIENTED_EDGE('',*,*,#2733,.F.);
#3842=ORIENTED_EDGE('',*,*,#2734,.F.);
#3843=ORIENTED_EDGE('',*,*,#2735,.F.);
#3844=ORIENTED_EDGE('',*,*,#2736,.F.);
#3845=ORIENTED_EDGE('',*,*,#2737,.F.);
#3846=ORIENTED_EDGE('',*,*,#2738,.F.);
#3847=ORIENTED_EDGE('',*,*,#2739,.F.);
#3848=ORIENTED_EDGE('',*,*,#2740,.F.);
#3849=ORIENTED_EDGE('',*,*,#2741,.F.);
#3850=ORIENTED_EDGE('',*,*,#2742,.F.);
#3851=ORIENTED_EDGE('',*,*,#2743,.F.);
#3852=ORIENTED_EDGE('',*,*,#2744,.F.);
#3853=ORIENTED_EDGE('',*,*,#2745,.F.);
#3854=ORIENTED_EDGE('',*,*,#2746,.F.);
#3855=ORIENTED_EDGE('',*,*,#2747,.F.);
#3856=ORIENTED_EDGE('',*,*,#2748,.F.);
#3857=ORIENTED_EDGE('',*,*,#2749,.F.);
#3858=ORIENTED_EDGE('',*,*,#2750,.F.);
#3859=ORIENTED_EDGE('',*,*,#2751,.F.);
#3860=ORIENTED_EDGE('',*,*,#2752,.F.);
#3861=ORIENTED_EDGE('',*,*,#2753,.F.);
#3862=ORIENTED_EDGE('',*,*,#2754,.F.);
#3863=ORIENTED_EDGE('',*,*,#2755,.F.);
#3864=ORIENTED_EDGE('',*,*,#2756,.F.);
#3865=ORIENTED_EDGE('',*,*,#2757,.F.);
#3866=ORIENTED_EDGE('',*,*,#2758,.F.);
#3867=ORIENTED_EDGE('',*,*,#2759,.F.);
#3868=ORIENTED_EDGE('',*,*,#2760,.F.);
#3869=ORIENTED_EDGE('',*,*,#2761,.F.);
#3870=ORIENTED_EDGE('',*,*,#2762,.F.);
#3871=ORIENTED_EDGE('',*,*,#2763,.F.);
#3872=ORIENTED_EDGE('',*,*,#2764,.F.);
#3873=ORIENTED_EDGE('',*,*,#2765,.F.);
#3874=ORIENTED_EDGE('',*,*,#2766,.F.);
#3875=ORIENTED_EDGE('',*,*,#2767,.F.);
#3876=ORIENTED_EDGE('',*,*,#2768,.F.);
#3877=ORIENTED_EDGE('',*,*,#2769,.F.);
#3878=ORIENTED_EDGE('',*,*,#2770,.F.);
#3879=ORIENTED_EDGE('',*,*,#2771,.F.);
#3880=ORIENTED_EDGE('',*,*,#2772,.F.);
#3881=ORIENTED_EDGE('',*,*,#2773,.F.);
#3882=ORIENTED_EDGE('',*,*,#2774,.F.);
#3883=ORIENTED_EDGE('',*,*,#2775,.F.);
#3884=ORIENTED_EDGE('',*,*,#2776,.F.);
#3885=ORIENTED_EDGE('',*,*,#2777,.F.);
#3886=ORIENTED_EDGE('',*,*,#2778,.F.);
#3887=ORIENTED_EDGE('',*,*,#2779,.F.);
#3888=ORIENTED_EDGE('',*,*,#2780,.F.);
#3889=ORIENTED_EDGE('',*,*,#2781,.F.);
#3890=ORIENTED_EDGE('',*,*,#2782,.F.);
#3891=ORIENTED_EDGE('',*,*,#2783,.F.);
#3892=ORIENTED_EDGE('',*,*,#2784,.F.);
#3893=ORIENTED_EDGE('',*,*,#2785,.F.);
#3894=ORIENTED_EDGE('',*,*,#2786,.F.);
#3895=ORIENTED_EDGE('',*,*,#2787,.F.);
#3896=ORIENTED_EDGE('',*,*,#2788,.F.);
#3897=ORIENTED_EDGE('',*,*,#2789,.F.);
#3898=ORIENTED_EDGE('',*,*,#2790,.F.);
#3899=ORIENTED_EDGE('',*,*,#2791,.F.);
#3900=ORIENTED_EDGE('',*,*,#2792,.F.);
#3901=ORIENTED_EDGE('',*,*,#2793,.F.);
#3902=ORIENTED_EDGE('',*,*,#2794,.F.);
#3903=ORIENTED_EDGE('',*,*,#2795,.F.);
#3904=ORIENTED_EDGE('',*,*,#2796,.F.);
#3905=ORIENTED_EDGE('',*,*,#2797,.F.);
#3906=ORIENTED_EDGE('',*,*,#2798,.F.);
#3907=ORIENTED_EDGE('',*,*,#2799,.F.);
#3908=ORIENTED_EDGE('',*,*,#2800,.F.);
#3909=ORIENTED_EDGE('',*,*,#2801,.F.);
#3910=ORIENTED_EDGE('',*,*,#2802,.F.);
#3911=ORIENTED_EDGE('',*,*,#2803,.F.);
#3912=ORIENTED_EDGE('',*,*,#2804,.F.);
#3913=ORIENTED_EDGE('',*,*,#2805,.F.);
#3914=ORIENTED_EDGE('',*,*,#2806,.F.);
#3915=ORIENTED_EDGE('',*,*,#2807,.F.);
#3916=ORIENTED_EDGE('',*,*,#2808,.F.);
#3917=ORIENTED_EDGE('',*,*,#2809,.F.);
#3918=ORIENTED_EDGE('',*,*,#2810,.F.);
#3919=ORIENTED_EDGE('',*,*,#2811,.F.);
#3920=ORIENTED_EDGE('',*,*,#2812,.F.);
#3921=ORIENTED_EDGE('',*,*,#2813,.F.);
#3922=ORIENTED_EDGE('',*,*,#2814,.F.);
#3923=ORIENTED_EDGE('',*,*,#2815,.F.);
#3924=ORIENTED_EDGE('',*,*,#2816,.F.);
#3925=ORIENTED_EDGE('',*,*,#2817,.F.);
#3926=ORIENTED_EDGE('',*,*,#2818,.F.);
#3927=ORIENTED_EDGE('',*,*,#2819,.F.);
#3928=ORIENTED_EDGE('',*,*,#2820,.F.);
#3929=ORIENTED_EDGE('',*,*,#2821,.F.);
#3930=ORIENTED_EDGE('',*,*,#2822,.F.);
#3931=ORIENTED_EDGE('',*,*,#2823,.F.);
#3932=ORIENTED_EDGE('',*,*,#2824,.F.);
#3933=ORIENTED_EDGE('',*,*,#2825,.F.);
#3934=ORIENTED_EDGE('',*,*,#2826,.F.);
#3935=ORIENTED_EDGE('',*,*,#2827,.T.);
#3936=ORIENTED_EDGE('',*,*,#2828,.T.);
#3937=ORIENTED_EDGE('',*,*,#2829,.T.);
#3938=ORIENTED_EDGE('',*,*,#2830,.T.);
#3939=ORIENTED_EDGE('',*,*,#2831,.T.);
#3940=ORIENTED_EDGE('',*,*,#2832,.T.);
#3941=ORIENTED_EDGE('',*,*,#2833,.T.);
#3942=ORIENTED_EDGE('',*,*,#2834,.T.);
#3943=ORIENTED_EDGE('',*,*,#2835,.T.);
#3944=ORIENTED_EDGE('',*,*,#2836,.T.);
#3945=ORIENTED_EDGE('',*,*,#2837,.T.);
#3946=ORIENTED_EDGE('',*,*,#2838,.T.);
#3947=ORIENTED_EDGE('',*,*,#2839,.T.);
#3948=ORIENTED_EDGE('',*,*,#2840,.T.);
#3949=ORIENTED_EDGE('',*,*,#2841,.T.);
#3950=ORIENTED_EDGE('',*,*,#2842,.T.);
#3951=ORIENTED_EDGE('',*,*,#2843,.T.);
#3952=ORIENTED_EDGE('',*,*,#2844,.T.);
#3953=ORIENTED_EDGE('',*,*,#2845,.T.);
#3954=ORIENTED_EDGE('',*,*,#2846,.T.);
#3955=ORIENTED_EDGE('',*,*,#2847,.T.);
#3956=ORIENTED_EDGE('',*,*,#2848,.T.);
#3957=ORIENTED_EDGE('',*,*,#2849,.T.);
#3958=ORIENTED_EDGE('',*,*,#2850,.T.);
#3959=ORIENTED_EDGE('',*,*,#2851,.T.);
#3960=ORIENTED_EDGE('',*,*,#2852,.T.);
#3961=ORIENTED_EDGE('',*,*,#2853,.T.);
#3962=ORIENTED_EDGE('',*,*,#2854,.T.);
#3963=ORIENTED_EDGE('',*,*,#2855,.T.);
#3964=ORIENTED_EDGE('',*,*,#2856,.T.);
#3965=ORIENTED_EDGE('',*,*,#2857,.T.);
#3966=ORIENTED_EDGE('',*,*,#2858,.T.);
#3967=ORIENTED_EDGE('',*,*,#2859,.T.);
#3968=ORIENTED_EDGE('',*,*,#2860,.T.);
#3969=ORIENTED_EDGE('',*,*,#2861,.T.);
#3970=ORIENTED_EDGE('',*,*,#2862,.T.);
#3971=ORIENTED_EDGE('',*,*,#2863,.T.);
#3972=ORIENTED_EDGE('',*,*,#2864,.T.);
#3973=ORIENTED_EDGE('',*,*,#2865,.T.);
#3974=ORIENTED_EDGE('',*,*,#2866,.T.);
#3975=ORIENTED_EDGE('',*,*,#2867,.T.);
#3976=ORIENTED_EDGE('',*,*,#2868,.T.);
#3977=ORIENTED_EDGE('',*,*,#2869,.T.);
#3978=ORIENTED_EDGE('',*,*,#2870,.T.);
#3979=ORIENTED_EDGE('',*,*,#2871,.T.);
#3980=ORIENTED_EDGE('',*,*,#2872,.T.);
#3981=ORIENTED_EDGE('',*,*,#2873,.T.);
#3982=ORIENTED_EDGE('',*,*,#2874,.T.);
#3983=ORIENTED_EDGE('',*,*,#2875,.T.);
#3984=ORIENTED_EDGE('',*,*,#2876,.T.);
#3985=ORIENTED_EDGE('',*,*,#2877,.T.);
#3986=ORIENTED_EDGE('',*,*,#2878,.T.);
#3987=ORIENTED_EDGE('',*,*,#2879,.T.);
#3988=ORIENTED_EDGE('',*,*,#2880,.T.);
#3989=ORIENTED_EDGE('',*,*,#2881,.T.);
#3990=ORIENTED_EDGE('',*,*,#2882,.T.);
#3991=ORIENTED_EDGE('',*,*,#2883,.T.);
#3992=ORIENTED_EDGE('',*,*,#2884,.T.);
#3993=ORIENTED_EDGE('',*,*,#2885,.T.);
#3994=ORIENTED_EDGE('',*,*,#2886,.T.);
#3995=ORIENTED_EDGE('',*,*,#2887,.T.);
#3996=ORIENTED_EDGE('',*,*,#2888,.T.);
#3997=ORIENTED_EDGE('',*,*,#2889,.T.);
#3998=ORIENTED_EDGE('',*,*,#2890,.T.);
#3999=ORIENTED_EDGE('',*,*,#2891,.T.);
#4000=ORIENTED_EDGE('',*,*,#2892,.T.);
#4001=ORIENTED_EDGE('',*,*,#2893,.T.);
#4002=ORIENTED_EDGE('',*,*,#2894,.T.);
#4003=ORIENTED_EDGE('',*,*,#2895,.T.);
#4004=ORIENTED_EDGE('',*,*,#2896,.T.);
#4005=ORIENTED_EDGE('',*,*,#2897,.T.);
#4006=ORIENTED_EDGE('',*,*,#2898,.T.);
#4007=ORIENTED_EDGE('',*,*,#2899,.T.);
#4008=ORIENTED_EDGE('',*,*,#2900,.T.);
#4009=ORIENTED_EDGE('',*,*,#2901,.T.);
#4010=ORIENTED_EDGE('',*,*,#2902,.T.);
#4011=ORIENTED_EDGE('',*,*,#2903,.T.);
#4012=ORIENTED_EDGE('',*,*,#2904,.T.);
#4013=ORIENTED_EDGE('',*,*,#2905,.T.);
#4014=ORIENTED_EDGE('',*,*,#2906,.T.);
#4015=ORIENTED_EDGE('',*,*,#2907,.T.);
#4016=ORIENTED_EDGE('',*,*,#2908,.T.);
#4017=ORIENTED_EDGE('',*,*,#2909,.T.);
#4018=ORIENTED_EDGE('',*,*,#2910,.T.);
#4019=ORIENTED_EDGE('',*,*,#2911,.T.);
#4020=ORIENTED_EDGE('',*,*,#2912,.T.);
#4021=ORIENTED_EDGE('',*,*,#2913,.T.);
#4022=ORIENTED_EDGE('',*,*,#2914,.T.);
#4023=ORIENTED_EDGE('',*,*,#2915,.T.);
#4024=ORIENTED_EDGE('',*,*,#2916,.T.);
#4025=ORIENTED_EDGE('',*,*,#2917,.T.);
#4026=ORIENTED_EDGE('',*,*,#2918,.T.);
#4027=ORIENTED_EDGE('',*,*,#2919,.T.);
#4028=ORIENTED_EDGE('',*,*,#2920,.T.);
#4029=ORIENTED_EDGE('',*,*,#2921,.T.);
#4030=ORIENTED_EDGE('',*,*,#2922,.T.);
#4031=ORIENTED_EDGE('',*,*,#2923,.T.);
#4032=ORIENTED_EDGE('',*,*,#2924,.T.);
#4033=ORIENTED_EDGE('',*,*,#2925,.T.);
#4034=ORIENTED_EDGE('',*,*,#2926,.T.);
#4035=ORIENTED_EDGE('',*,*,#2927,.T.);
#4036=ORIENTED_EDGE('',*,*,#2928,.T.);
#4037=ORIENTED_EDGE('',*,*,#2929,.T.);
#4038=ORIENTED_EDGE('',*,*,#2930,.T.);
#4039=ORIENTED_EDGE('',*,*,#2931,.F.);
#4040=ORIENTED_EDGE('',*,*,#2932,.F.);
#4041=ORIENTED_EDGE('',*,*,#2933,.F.);
#4042=ORIENTED_EDGE('',*,*,#2934,.F.);
#4043=ORIENTED_EDGE('',*,*,#2935,.F.);
#4044=ORIENTED_EDGE('',*,*,#2936,.F.);
#4045=ORIENTED_EDGE('',*,*,#2930,.F.);
#4046=ORIENTED_EDGE('',*,*,#2937,.T.);
#4047=ORIENTED_EDGE('',*,*,#2938,.T.);
#4048=ORIENTED_EDGE('',*,*,#2937,.F.);
#4049=ORIENTED_EDGE('',*,*,#2934,.T.);
#4050=ORIENTED_EDGE('',*,*,#2939,.T.);
#4051=ORIENTED_EDGE('',*,*,#2940,.F.);
#4052=ORIENTED_EDGE('',*,*,#2941,.F.);
#4053=ORIENTED_EDGE('',*,*,#2933,.T.);
#4054=ORIENTED_EDGE('',*,*,#2942,.T.);
#4055=ORIENTED_EDGE('',*,*,#2943,.F.);
#4056=ORIENTED_EDGE('',*,*,#2939,.F.);
#4057=ORIENTED_EDGE('',*,*,#2932,.T.);
#4058=ORIENTED_EDGE('',*,*,#2944,.T.);
#4059=ORIENTED_EDGE('',*,*,#2945,.F.);
#4060=ORIENTED_EDGE('',*,*,#2942,.F.);
#4061=ORIENTED_EDGE('',*,*,#2938,.F.);
#4062=ORIENTED_EDGE('',*,*,#2946,.T.);
#4063=ORIENTED_EDGE('',*,*,#2511,.T.);
#4064=ORIENTED_EDGE('',*,*,#2947,.T.);
#4065=ORIENTED_EDGE('',*,*,#2948,.T.);
#4066=ORIENTED_EDGE('',*,*,#2949,.T.);
#4067=ORIENTED_EDGE('',*,*,#2826,.T.);
#4068=ORIENTED_EDGE('',*,*,#2950,.T.);
#4069=ORIENTED_EDGE('',*,*,#2931,.T.);
#4070=ORIENTED_EDGE('',*,*,#2951,.T.);
#4071=ORIENTED_EDGE('',*,*,#2952,.F.);
#4072=ORIENTED_EDGE('',*,*,#2944,.F.);
#4073=ORIENTED_EDGE('',*,*,#2935,.T.);
#4074=ORIENTED_EDGE('',*,*,#2941,.T.);
#4075=ORIENTED_EDGE('',*,*,#2953,.F.);
#4076=ORIENTED_EDGE('',*,*,#2954,.F.);
#4077=ORIENTED_EDGE('',*,*,#2936,.T.);
#4078=ORIENTED_EDGE('',*,*,#2954,.T.);
#4079=ORIENTED_EDGE('',*,*,#2955,.F.);
#4080=ORIENTED_EDGE('',*,*,#2951,.F.);
#4081=ORIENTED_EDGE('',*,*,#2955,.T.);
#4082=ORIENTED_EDGE('',*,*,#2953,.T.);
#4083=ORIENTED_EDGE('',*,*,#2940,.T.);
#4084=ORIENTED_EDGE('',*,*,#2943,.T.);
#4085=ORIENTED_EDGE('',*,*,#2945,.T.);
#4086=ORIENTED_EDGE('',*,*,#2952,.T.);
#4087=ORIENTED_EDGE('',*,*,#2956,.F.);
#4088=ORIENTED_EDGE('',*,*,#2615,.F.);
#4089=ORIENTED_EDGE('',*,*,#2614,.F.);
#4090=ORIENTED_EDGE('',*,*,#2613,.F.);
#4091=ORIENTED_EDGE('',*,*,#2612,.F.);
#4092=ORIENTED_EDGE('',*,*,#2611,.F.);
#4093=ORIENTED_EDGE('',*,*,#2610,.F.);
#4094=ORIENTED_EDGE('',*,*,#2609,.F.);
#4095=ORIENTED_EDGE('',*,*,#2608,.F.);
#4096=ORIENTED_EDGE('',*,*,#2607,.F.);
#4097=ORIENTED_EDGE('',*,*,#2606,.F.);
#4098=ORIENTED_EDGE('',*,*,#2605,.F.);
#4099=ORIENTED_EDGE('',*,*,#2604,.F.);
#4100=ORIENTED_EDGE('',*,*,#2603,.F.);
#4101=ORIENTED_EDGE('',*,*,#2602,.F.);
#4102=ORIENTED_EDGE('',*,*,#2601,.F.);
#4103=ORIENTED_EDGE('',*,*,#2600,.F.);
#4104=ORIENTED_EDGE('',*,*,#2599,.F.);
#4105=ORIENTED_EDGE('',*,*,#2598,.F.);
#4106=ORIENTED_EDGE('',*,*,#2597,.F.);
#4107=ORIENTED_EDGE('',*,*,#2596,.F.);
#4108=ORIENTED_EDGE('',*,*,#2595,.F.);
#4109=ORIENTED_EDGE('',*,*,#2594,.F.);
#4110=ORIENTED_EDGE('',*,*,#2593,.F.);
#4111=ORIENTED_EDGE('',*,*,#2592,.F.);
#4112=ORIENTED_EDGE('',*,*,#2591,.F.);
#4113=ORIENTED_EDGE('',*,*,#2590,.F.);
#4114=ORIENTED_EDGE('',*,*,#2589,.F.);
#4115=ORIENTED_EDGE('',*,*,#2588,.F.);
#4116=ORIENTED_EDGE('',*,*,#2587,.F.);
#4117=ORIENTED_EDGE('',*,*,#2586,.F.);
#4118=ORIENTED_EDGE('',*,*,#2585,.F.);
#4119=ORIENTED_EDGE('',*,*,#2584,.F.);
#4120=ORIENTED_EDGE('',*,*,#2583,.F.);
#4121=ORIENTED_EDGE('',*,*,#2582,.F.);
#4122=ORIENTED_EDGE('',*,*,#2581,.F.);
#4123=ORIENTED_EDGE('',*,*,#2580,.F.);
#4124=ORIENTED_EDGE('',*,*,#2579,.F.);
#4125=ORIENTED_EDGE('',*,*,#2578,.F.);
#4126=ORIENTED_EDGE('',*,*,#2577,.F.);
#4127=ORIENTED_EDGE('',*,*,#2576,.F.);
#4128=ORIENTED_EDGE('',*,*,#2575,.F.);
#4129=ORIENTED_EDGE('',*,*,#2574,.F.);
#4130=ORIENTED_EDGE('',*,*,#2573,.F.);
#4131=ORIENTED_EDGE('',*,*,#2572,.F.);
#4132=ORIENTED_EDGE('',*,*,#2571,.F.);
#4133=ORIENTED_EDGE('',*,*,#2570,.F.);
#4134=ORIENTED_EDGE('',*,*,#2569,.F.);
#4135=ORIENTED_EDGE('',*,*,#2568,.F.);
#4136=ORIENTED_EDGE('',*,*,#2567,.F.);
#4137=ORIENTED_EDGE('',*,*,#2566,.F.);
#4138=ORIENTED_EDGE('',*,*,#2565,.F.);
#4139=ORIENTED_EDGE('',*,*,#2564,.F.);
#4140=ORIENTED_EDGE('',*,*,#2563,.F.);
#4141=ORIENTED_EDGE('',*,*,#2562,.F.);
#4142=ORIENTED_EDGE('',*,*,#2561,.F.);
#4143=ORIENTED_EDGE('',*,*,#2560,.F.);
#4144=ORIENTED_EDGE('',*,*,#2559,.F.);
#4145=ORIENTED_EDGE('',*,*,#2558,.F.);
#4146=ORIENTED_EDGE('',*,*,#2557,.F.);
#4147=ORIENTED_EDGE('',*,*,#2556,.F.);
#4148=ORIENTED_EDGE('',*,*,#2555,.F.);
#4149=ORIENTED_EDGE('',*,*,#2554,.F.);
#4150=ORIENTED_EDGE('',*,*,#2553,.F.);
#4151=ORIENTED_EDGE('',*,*,#2552,.F.);
#4152=ORIENTED_EDGE('',*,*,#2551,.F.);
#4153=ORIENTED_EDGE('',*,*,#2550,.F.);
#4154=ORIENTED_EDGE('',*,*,#2549,.F.);
#4155=ORIENTED_EDGE('',*,*,#2548,.F.);
#4156=ORIENTED_EDGE('',*,*,#2547,.F.);
#4157=ORIENTED_EDGE('',*,*,#2546,.F.);
#4158=ORIENTED_EDGE('',*,*,#2545,.F.);
#4159=ORIENTED_EDGE('',*,*,#2544,.F.);
#4160=ORIENTED_EDGE('',*,*,#2543,.F.);
#4161=ORIENTED_EDGE('',*,*,#2542,.F.);
#4162=ORIENTED_EDGE('',*,*,#2541,.F.);
#4163=ORIENTED_EDGE('',*,*,#2540,.F.);
#4164=ORIENTED_EDGE('',*,*,#2539,.F.);
#4165=ORIENTED_EDGE('',*,*,#2538,.F.);
#4166=ORIENTED_EDGE('',*,*,#2537,.F.);
#4167=ORIENTED_EDGE('',*,*,#2536,.F.);
#4168=ORIENTED_EDGE('',*,*,#2535,.F.);
#4169=ORIENTED_EDGE('',*,*,#2534,.F.);
#4170=ORIENTED_EDGE('',*,*,#2533,.F.);
#4171=ORIENTED_EDGE('',*,*,#2532,.F.);
#4172=ORIENTED_EDGE('',*,*,#2531,.F.);
#4173=ORIENTED_EDGE('',*,*,#2530,.F.);
#4174=ORIENTED_EDGE('',*,*,#2529,.F.);
#4175=ORIENTED_EDGE('',*,*,#2528,.F.);
#4176=ORIENTED_EDGE('',*,*,#2527,.F.);
#4177=ORIENTED_EDGE('',*,*,#2526,.F.);
#4178=ORIENTED_EDGE('',*,*,#2525,.F.);
#4179=ORIENTED_EDGE('',*,*,#2524,.F.);
#4180=ORIENTED_EDGE('',*,*,#2523,.F.);
#4181=ORIENTED_EDGE('',*,*,#2522,.F.);
#4182=ORIENTED_EDGE('',*,*,#2521,.F.);
#4183=ORIENTED_EDGE('',*,*,#2520,.F.);
#4184=ORIENTED_EDGE('',*,*,#2519,.F.);
#4185=ORIENTED_EDGE('',*,*,#2518,.F.);
#4186=ORIENTED_EDGE('',*,*,#2517,.F.);
#4187=ORIENTED_EDGE('',*,*,#2516,.F.);
#4188=ORIENTED_EDGE('',*,*,#2515,.F.);
#4189=ORIENTED_EDGE('',*,*,#2514,.F.);
#4190=ORIENTED_EDGE('',*,*,#2513,.F.);
#4191=ORIENTED_EDGE('',*,*,#2512,.F.);
#4192=ORIENTED_EDGE('',*,*,#2946,.F.);
#4193=ORIENTED_EDGE('',*,*,#2950,.F.);
#4194=ORIENTED_EDGE('',*,*,#2825,.T.);
#4195=ORIENTED_EDGE('',*,*,#2824,.T.);
#4196=ORIENTED_EDGE('',*,*,#2823,.T.);
#4197=ORIENTED_EDGE('',*,*,#2822,.T.);
#4198=ORIENTED_EDGE('',*,*,#2821,.T.);
#4199=ORIENTED_EDGE('',*,*,#2820,.T.);
#4200=ORIENTED_EDGE('',*,*,#2819,.T.);
#4201=ORIENTED_EDGE('',*,*,#2818,.T.);
#4202=ORIENTED_EDGE('',*,*,#2817,.T.);
#4203=ORIENTED_EDGE('',*,*,#2816,.T.);
#4204=ORIENTED_EDGE('',*,*,#2815,.T.);
#4205=ORIENTED_EDGE('',*,*,#2814,.T.);
#4206=ORIENTED_EDGE('',*,*,#2813,.T.);
#4207=ORIENTED_EDGE('',*,*,#2812,.T.);
#4208=ORIENTED_EDGE('',*,*,#2811,.T.);
#4209=ORIENTED_EDGE('',*,*,#2810,.T.);
#4210=ORIENTED_EDGE('',*,*,#2809,.T.);
#4211=ORIENTED_EDGE('',*,*,#2808,.T.);
#4212=ORIENTED_EDGE('',*,*,#2807,.T.);
#4213=ORIENTED_EDGE('',*,*,#2806,.T.);
#4214=ORIENTED_EDGE('',*,*,#2805,.T.);
#4215=ORIENTED_EDGE('',*,*,#2804,.T.);
#4216=ORIENTED_EDGE('',*,*,#2803,.T.);
#4217=ORIENTED_EDGE('',*,*,#2802,.T.);
#4218=ORIENTED_EDGE('',*,*,#2801,.T.);
#4219=ORIENTED_EDGE('',*,*,#2800,.T.);
#4220=ORIENTED_EDGE('',*,*,#2799,.T.);
#4221=ORIENTED_EDGE('',*,*,#2798,.T.);
#4222=ORIENTED_EDGE('',*,*,#2797,.T.);
#4223=ORIENTED_EDGE('',*,*,#2796,.T.);
#4224=ORIENTED_EDGE('',*,*,#2795,.T.);
#4225=ORIENTED_EDGE('',*,*,#2794,.T.);
#4226=ORIENTED_EDGE('',*,*,#2793,.T.);
#4227=ORIENTED_EDGE('',*,*,#2792,.T.);
#4228=ORIENTED_EDGE('',*,*,#2791,.T.);
#4229=ORIENTED_EDGE('',*,*,#2790,.T.);
#4230=ORIENTED_EDGE('',*,*,#2789,.T.);
#4231=ORIENTED_EDGE('',*,*,#2788,.T.);
#4232=ORIENTED_EDGE('',*,*,#2787,.T.);
#4233=ORIENTED_EDGE('',*,*,#2786,.T.);
#4234=ORIENTED_EDGE('',*,*,#2785,.T.);
#4235=ORIENTED_EDGE('',*,*,#2784,.T.);
#4236=ORIENTED_EDGE('',*,*,#2783,.T.);
#4237=ORIENTED_EDGE('',*,*,#2782,.T.);
#4238=ORIENTED_EDGE('',*,*,#2781,.T.);
#4239=ORIENTED_EDGE('',*,*,#2780,.T.);
#4240=ORIENTED_EDGE('',*,*,#2779,.T.);
#4241=ORIENTED_EDGE('',*,*,#2778,.T.);
#4242=ORIENTED_EDGE('',*,*,#2777,.T.);
#4243=ORIENTED_EDGE('',*,*,#2776,.T.);
#4244=ORIENTED_EDGE('',*,*,#2775,.T.);
#4245=ORIENTED_EDGE('',*,*,#2774,.T.);
#4246=ORIENTED_EDGE('',*,*,#2773,.T.);
#4247=ORIENTED_EDGE('',*,*,#2772,.T.);
#4248=ORIENTED_EDGE('',*,*,#2771,.T.);
#4249=ORIENTED_EDGE('',*,*,#2770,.T.);
#4250=ORIENTED_EDGE('',*,*,#2769,.T.);
#4251=ORIENTED_EDGE('',*,*,#2768,.T.);
#4252=ORIENTED_EDGE('',*,*,#2767,.T.);
#4253=ORIENTED_EDGE('',*,*,#2766,.T.);
#4254=ORIENTED_EDGE('',*,*,#2765,.T.);
#4255=ORIENTED_EDGE('',*,*,#2764,.T.);
#4256=ORIENTED_EDGE('',*,*,#2763,.T.);
#4257=ORIENTED_EDGE('',*,*,#2762,.T.);
#4258=ORIENTED_EDGE('',*,*,#2761,.T.);
#4259=ORIENTED_EDGE('',*,*,#2760,.T.);
#4260=ORIENTED_EDGE('',*,*,#2759,.T.);
#4261=ORIENTED_EDGE('',*,*,#2758,.T.);
#4262=ORIENTED_EDGE('',*,*,#2757,.T.);
#4263=ORIENTED_EDGE('',*,*,#2756,.T.);
#4264=ORIENTED_EDGE('',*,*,#2755,.T.);
#4265=ORIENTED_EDGE('',*,*,#2754,.T.);
#4266=ORIENTED_EDGE('',*,*,#2753,.T.);
#4267=ORIENTED_EDGE('',*,*,#2752,.T.);
#4268=ORIENTED_EDGE('',*,*,#2751,.T.);
#4269=ORIENTED_EDGE('',*,*,#2750,.T.);
#4270=ORIENTED_EDGE('',*,*,#2749,.T.);
#4271=ORIENTED_EDGE('',*,*,#2748,.T.);
#4272=ORIENTED_EDGE('',*,*,#2747,.T.);
#4273=ORIENTED_EDGE('',*,*,#2746,.T.);
#4274=ORIENTED_EDGE('',*,*,#2745,.T.);
#4275=ORIENTED_EDGE('',*,*,#2744,.T.);
#4276=ORIENTED_EDGE('',*,*,#2743,.T.);
#4277=ORIENTED_EDGE('',*,*,#2742,.T.);
#4278=ORIENTED_EDGE('',*,*,#2741,.T.);
#4279=ORIENTED_EDGE('',*,*,#2740,.T.);
#4280=ORIENTED_EDGE('',*,*,#2739,.T.);
#4281=ORIENTED_EDGE('',*,*,#2738,.T.);
#4282=ORIENTED_EDGE('',*,*,#2737,.T.);
#4283=ORIENTED_EDGE('',*,*,#2736,.T.);
#4284=ORIENTED_EDGE('',*,*,#2735,.T.);
#4285=ORIENTED_EDGE('',*,*,#2734,.T.);
#4286=ORIENTED_EDGE('',*,*,#2733,.T.);
#4287=ORIENTED_EDGE('',*,*,#2732,.T.);
#4288=ORIENTED_EDGE('',*,*,#2731,.T.);
#4289=ORIENTED_EDGE('',*,*,#2730,.T.);
#4290=ORIENTED_EDGE('',*,*,#2729,.T.);
#4291=ORIENTED_EDGE('',*,*,#2728,.T.);
#4292=ORIENTED_EDGE('',*,*,#2727,.T.);
#4293=ORIENTED_EDGE('',*,*,#2726,.T.);
#4294=ORIENTED_EDGE('',*,*,#2725,.T.);
#4295=ORIENTED_EDGE('',*,*,#2724,.T.);
#4296=ORIENTED_EDGE('',*,*,#2723,.T.);
#4297=ORIENTED_EDGE('',*,*,#2722,.T.);
#4298=ORIENTED_EDGE('',*,*,#2957,.F.);
#4299=ORIENTED_EDGE('',*,*,#2720,.F.);
#4300=ORIENTED_EDGE('',*,*,#2929,.F.);
#4301=ORIENTED_EDGE('',*,*,#2928,.F.);
#4302=ORIENTED_EDGE('',*,*,#2927,.F.);
#4303=ORIENTED_EDGE('',*,*,#2926,.F.);
#4304=ORIENTED_EDGE('',*,*,#2925,.F.);
#4305=ORIENTED_EDGE('',*,*,#2924,.F.);
#4306=ORIENTED_EDGE('',*,*,#2923,.F.);
#4307=ORIENTED_EDGE('',*,*,#2922,.F.);
#4308=ORIENTED_EDGE('',*,*,#2921,.F.);
#4309=ORIENTED_EDGE('',*,*,#2920,.F.);
#4310=ORIENTED_EDGE('',*,*,#2919,.F.);
#4311=ORIENTED_EDGE('',*,*,#2918,.F.);
#4312=ORIENTED_EDGE('',*,*,#2917,.F.);
#4313=ORIENTED_EDGE('',*,*,#2916,.F.);
#4314=ORIENTED_EDGE('',*,*,#2915,.F.);
#4315=ORIENTED_EDGE('',*,*,#2914,.F.);
#4316=ORIENTED_EDGE('',*,*,#2913,.F.);
#4317=ORIENTED_EDGE('',*,*,#2912,.F.);
#4318=ORIENTED_EDGE('',*,*,#2911,.F.);
#4319=ORIENTED_EDGE('',*,*,#2910,.F.);
#4320=ORIENTED_EDGE('',*,*,#2909,.F.);
#4321=ORIENTED_EDGE('',*,*,#2908,.F.);
#4322=ORIENTED_EDGE('',*,*,#2907,.F.);
#4323=ORIENTED_EDGE('',*,*,#2906,.F.);
#4324=ORIENTED_EDGE('',*,*,#2905,.F.);
#4325=ORIENTED_EDGE('',*,*,#2904,.F.);
#4326=ORIENTED_EDGE('',*,*,#2903,.F.);
#4327=ORIENTED_EDGE('',*,*,#2902,.F.);
#4328=ORIENTED_EDGE('',*,*,#2901,.F.);
#4329=ORIENTED_EDGE('',*,*,#2900,.F.);
#4330=ORIENTED_EDGE('',*,*,#2899,.F.);
#4331=ORIENTED_EDGE('',*,*,#2898,.F.);
#4332=ORIENTED_EDGE('',*,*,#2897,.F.);
#4333=ORIENTED_EDGE('',*,*,#2896,.F.);
#4334=ORIENTED_EDGE('',*,*,#2895,.F.);
#4335=ORIENTED_EDGE('',*,*,#2894,.F.);
#4336=ORIENTED_EDGE('',*,*,#2893,.F.);
#4337=ORIENTED_EDGE('',*,*,#2892,.F.);
#4338=ORIENTED_EDGE('',*,*,#2891,.F.);
#4339=ORIENTED_EDGE('',*,*,#2890,.F.);
#4340=ORIENTED_EDGE('',*,*,#2889,.F.);
#4341=ORIENTED_EDGE('',*,*,#2888,.F.);
#4342=ORIENTED_EDGE('',*,*,#2887,.F.);
#4343=ORIENTED_EDGE('',*,*,#2886,.F.);
#4344=ORIENTED_EDGE('',*,*,#2885,.F.);
#4345=ORIENTED_EDGE('',*,*,#2884,.F.);
#4346=ORIENTED_EDGE('',*,*,#2883,.F.);
#4347=ORIENTED_EDGE('',*,*,#2882,.F.);
#4348=ORIENTED_EDGE('',*,*,#2881,.F.);
#4349=ORIENTED_EDGE('',*,*,#2880,.F.);
#4350=ORIENTED_EDGE('',*,*,#2879,.F.);
#4351=ORIENTED_EDGE('',*,*,#2878,.F.);
#4352=ORIENTED_EDGE('',*,*,#2877,.F.);
#4353=ORIENTED_EDGE('',*,*,#2876,.F.);
#4354=ORIENTED_EDGE('',*,*,#2875,.F.);
#4355=ORIENTED_EDGE('',*,*,#2874,.F.);
#4356=ORIENTED_EDGE('',*,*,#2873,.F.);
#4357=ORIENTED_EDGE('',*,*,#2872,.F.);
#4358=ORIENTED_EDGE('',*,*,#2871,.F.);
#4359=ORIENTED_EDGE('',*,*,#2870,.F.);
#4360=ORIENTED_EDGE('',*,*,#2869,.F.);
#4361=ORIENTED_EDGE('',*,*,#2868,.F.);
#4362=ORIENTED_EDGE('',*,*,#2867,.F.);
#4363=ORIENTED_EDGE('',*,*,#2866,.F.);
#4364=ORIENTED_EDGE('',*,*,#2865,.F.);
#4365=ORIENTED_EDGE('',*,*,#2864,.F.);
#4366=ORIENTED_EDGE('',*,*,#2863,.F.);
#4367=ORIENTED_EDGE('',*,*,#2862,.F.);
#4368=ORIENTED_EDGE('',*,*,#2861,.F.);
#4369=ORIENTED_EDGE('',*,*,#2860,.F.);
#4370=ORIENTED_EDGE('',*,*,#2859,.F.);
#4371=ORIENTED_EDGE('',*,*,#2858,.F.);
#4372=ORIENTED_EDGE('',*,*,#2857,.F.);
#4373=ORIENTED_EDGE('',*,*,#2856,.F.);
#4374=ORIENTED_EDGE('',*,*,#2855,.F.);
#4375=ORIENTED_EDGE('',*,*,#2854,.F.);
#4376=ORIENTED_EDGE('',*,*,#2853,.F.);
#4377=ORIENTED_EDGE('',*,*,#2852,.F.);
#4378=ORIENTED_EDGE('',*,*,#2851,.F.);
#4379=ORIENTED_EDGE('',*,*,#2850,.F.);
#4380=ORIENTED_EDGE('',*,*,#2849,.F.);
#4381=ORIENTED_EDGE('',*,*,#2848,.F.);
#4382=ORIENTED_EDGE('',*,*,#2847,.F.);
#4383=ORIENTED_EDGE('',*,*,#2846,.F.);
#4384=ORIENTED_EDGE('',*,*,#2845,.F.);
#4385=ORIENTED_EDGE('',*,*,#2844,.F.);
#4386=ORIENTED_EDGE('',*,*,#2843,.F.);
#4387=ORIENTED_EDGE('',*,*,#2842,.F.);
#4388=ORIENTED_EDGE('',*,*,#2841,.F.);
#4389=ORIENTED_EDGE('',*,*,#2840,.F.);
#4390=ORIENTED_EDGE('',*,*,#2839,.F.);
#4391=ORIENTED_EDGE('',*,*,#2838,.F.);
#4392=ORIENTED_EDGE('',*,*,#2837,.F.);
#4393=ORIENTED_EDGE('',*,*,#2836,.F.);
#4394=ORIENTED_EDGE('',*,*,#2835,.F.);
#4395=ORIENTED_EDGE('',*,*,#2834,.F.);
#4396=ORIENTED_EDGE('',*,*,#2833,.F.);
#4397=ORIENTED_EDGE('',*,*,#2832,.F.);
#4398=ORIENTED_EDGE('',*,*,#2831,.F.);
#4399=ORIENTED_EDGE('',*,*,#2830,.F.);
#4400=ORIENTED_EDGE('',*,*,#2829,.F.);
#4401=ORIENTED_EDGE('',*,*,#2828,.F.);
#4402=ORIENTED_EDGE('',*,*,#2827,.F.);
#4403=ORIENTED_EDGE('',*,*,#2949,.F.);
#4404=ORIENTED_EDGE('',*,*,#2948,.F.);
#4405=ORIENTED_EDGE('',*,*,#2947,.F.);
#4406=ORIENTED_EDGE('',*,*,#2510,.F.);
#4407=ORIENTED_EDGE('',*,*,#2719,.F.);
#4408=ORIENTED_EDGE('',*,*,#2718,.F.);
#4409=ORIENTED_EDGE('',*,*,#2717,.F.);
#4410=ORIENTED_EDGE('',*,*,#2716,.F.);
#4411=ORIENTED_EDGE('',*,*,#2715,.F.);
#4412=ORIENTED_EDGE('',*,*,#2714,.F.);
#4413=ORIENTED_EDGE('',*,*,#2713,.F.);
#4414=ORIENTED_EDGE('',*,*,#2712,.F.);
#4415=ORIENTED_EDGE('',*,*,#2711,.F.);
#4416=ORIENTED_EDGE('',*,*,#2710,.F.);
#4417=ORIENTED_EDGE('',*,*,#2709,.F.);
#4418=ORIENTED_EDGE('',*,*,#2708,.F.);
#4419=ORIENTED_EDGE('',*,*,#2707,.F.);
#4420=ORIENTED_EDGE('',*,*,#2706,.F.);
#4421=ORIENTED_EDGE('',*,*,#2705,.F.);
#4422=ORIENTED_EDGE('',*,*,#2704,.F.);
#4423=ORIENTED_EDGE('',*,*,#2703,.F.);
#4424=ORIENTED_EDGE('',*,*,#2702,.F.);
#4425=ORIENTED_EDGE('',*,*,#2701,.F.);
#4426=ORIENTED_EDGE('',*,*,#2700,.F.);
#4427=ORIENTED_EDGE('',*,*,#2699,.F.);
#4428=ORIENTED_EDGE('',*,*,#2698,.F.);
#4429=ORIENTED_EDGE('',*,*,#2697,.F.);
#4430=ORIENTED_EDGE('',*,*,#2696,.F.);
#4431=ORIENTED_EDGE('',*,*,#2695,.F.);
#4432=ORIENTED_EDGE('',*,*,#2694,.F.);
#4433=ORIENTED_EDGE('',*,*,#2693,.F.);
#4434=ORIENTED_EDGE('',*,*,#2692,.F.);
#4435=ORIENTED_EDGE('',*,*,#2691,.F.);
#4436=ORIENTED_EDGE('',*,*,#2690,.F.);
#4437=ORIENTED_EDGE('',*,*,#2689,.F.);
#4438=ORIENTED_EDGE('',*,*,#2688,.F.);
#4439=ORIENTED_EDGE('',*,*,#2687,.F.);
#4440=ORIENTED_EDGE('',*,*,#2686,.F.);
#4441=ORIENTED_EDGE('',*,*,#2685,.F.);
#4442=ORIENTED_EDGE('',*,*,#2684,.F.);
#4443=ORIENTED_EDGE('',*,*,#2683,.F.);
#4444=ORIENTED_EDGE('',*,*,#2682,.F.);
#4445=ORIENTED_EDGE('',*,*,#2681,.F.);
#4446=ORIENTED_EDGE('',*,*,#2680,.F.);
#4447=ORIENTED_EDGE('',*,*,#2679,.F.);
#4448=ORIENTED_EDGE('',*,*,#2678,.F.);
#4449=ORIENTED_EDGE('',*,*,#2677,.F.);
#4450=ORIENTED_EDGE('',*,*,#2676,.F.);
#4451=ORIENTED_EDGE('',*,*,#2675,.F.);
#4452=ORIENTED_EDGE('',*,*,#2674,.F.);
#4453=ORIENTED_EDGE('',*,*,#2673,.F.);
#4454=ORIENTED_EDGE('',*,*,#2672,.F.);
#4455=ORIENTED_EDGE('',*,*,#2671,.F.);
#4456=ORIENTED_EDGE('',*,*,#2670,.F.);
#4457=ORIENTED_EDGE('',*,*,#2669,.F.);
#4458=ORIENTED_EDGE('',*,*,#2668,.F.);
#4459=ORIENTED_EDGE('',*,*,#2667,.F.);
#4460=ORIENTED_EDGE('',*,*,#2666,.F.);
#4461=ORIENTED_EDGE('',*,*,#2665,.F.);
#4462=ORIENTED_EDGE('',*,*,#2664,.F.);
#4463=ORIENTED_EDGE('',*,*,#2663,.F.);
#4464=ORIENTED_EDGE('',*,*,#2662,.F.);
#4465=ORIENTED_EDGE('',*,*,#2661,.F.);
#4466=ORIENTED_EDGE('',*,*,#2660,.F.);
#4467=ORIENTED_EDGE('',*,*,#2659,.F.);
#4468=ORIENTED_EDGE('',*,*,#2658,.F.);
#4469=ORIENTED_EDGE('',*,*,#2657,.F.);
#4470=ORIENTED_EDGE('',*,*,#2656,.F.);
#4471=ORIENTED_EDGE('',*,*,#2655,.F.);
#4472=ORIENTED_EDGE('',*,*,#2654,.F.);
#4473=ORIENTED_EDGE('',*,*,#2653,.F.);
#4474=ORIENTED_EDGE('',*,*,#2652,.F.);
#4475=ORIENTED_EDGE('',*,*,#2651,.F.);
#4476=ORIENTED_EDGE('',*,*,#2650,.F.);
#4477=ORIENTED_EDGE('',*,*,#2649,.F.);
#4478=ORIENTED_EDGE('',*,*,#2648,.F.);
#4479=ORIENTED_EDGE('',*,*,#2647,.F.);
#4480=ORIENTED_EDGE('',*,*,#2646,.F.);
#4481=ORIENTED_EDGE('',*,*,#2645,.F.);
#4482=ORIENTED_EDGE('',*,*,#2644,.F.);
#4483=ORIENTED_EDGE('',*,*,#2643,.F.);
#4484=ORIENTED_EDGE('',*,*,#2642,.F.);
#4485=ORIENTED_EDGE('',*,*,#2641,.F.);
#4486=ORIENTED_EDGE('',*,*,#2640,.F.);
#4487=ORIENTED_EDGE('',*,*,#2639,.F.);
#4488=ORIENTED_EDGE('',*,*,#2638,.F.);
#4489=ORIENTED_EDGE('',*,*,#2637,.F.);
#4490=ORIENTED_EDGE('',*,*,#2636,.F.);
#4491=ORIENTED_EDGE('',*,*,#2635,.F.);
#4492=ORIENTED_EDGE('',*,*,#2634,.F.);
#4493=ORIENTED_EDGE('',*,*,#2633,.F.);
#4494=ORIENTED_EDGE('',*,*,#2632,.F.);
#4495=ORIENTED_EDGE('',*,*,#2631,.F.);
#4496=ORIENTED_EDGE('',*,*,#2630,.F.);
#4497=ORIENTED_EDGE('',*,*,#2629,.F.);
#4498=ORIENTED_EDGE('',*,*,#2628,.F.);
#4499=ORIENTED_EDGE('',*,*,#2627,.F.);
#4500=ORIENTED_EDGE('',*,*,#2626,.F.);
#4501=ORIENTED_EDGE('',*,*,#2625,.F.);
#4502=ORIENTED_EDGE('',*,*,#2624,.F.);
#4503=ORIENTED_EDGE('',*,*,#2623,.F.);
#4504=ORIENTED_EDGE('',*,*,#2622,.F.);
#4505=ORIENTED_EDGE('',*,*,#2621,.F.);
#4506=ORIENTED_EDGE('',*,*,#2620,.F.);
#4507=ORIENTED_EDGE('',*,*,#2619,.F.);
#4508=ORIENTED_EDGE('',*,*,#2618,.F.);
#4509=ORIENTED_EDGE('',*,*,#2617,.F.);
#4510=ORIENTED_EDGE('',*,*,#2956,.T.);
#4511=ORIENTED_EDGE('',*,*,#2721,.T.);
#4512=ORIENTED_EDGE('',*,*,#2957,.T.);
#4513=ORIENTED_EDGE('',*,*,#2616,.T.);
#4575=CYLINDRICAL_SURFACE('',#5070,5.91675);
#4576=CYLINDRICAL_SURFACE('',#5073,4.91825);
#4577=CYLINDRICAL_SURFACE('',#5078,7.);
#4707=ADVANCED_FACE('',(#811),#4575,.T.);
#4708=ADVANCED_FACE('',(#812),#4576,.T.);
#4709=ADVANCED_FACE('',(#813,#607),#672,.T.);
#4710=ADVANCED_FACE('',(#814),#4577,.T.);
#4711=ADVANCED_FACE('',(#815),#673,.T.);
#4712=ADVANCED_FACE('',(#816),#674,.T.);
#4713=ADVANCED_FACE('',(#817),#675,.T.);
#4714=ADVANCED_FACE('',(#818,#608),#676,.F.);
#4715=ADVANCED_FACE('',(#819),#677,.T.);
#4716=ADVANCED_FACE('',(#820),#678,.T.);
#4717=ADVANCED_FACE('',(#821),#679,.T.);
#4718=ADVANCED_FACE('',(#822),#680,.T.);
#4719=ADVANCED_FACE('',(#823),#53,.F.);
#4720=ADVANCED_FACE('',(#824),#54,.F.);
#4721=ADVANCED_FACE('',(#825),#681,.F.);
#4730=CLOSED_SHELL('',(#4707,#4708,#4709,#4710,#4711,#4712,#4713,#4714,
#4715,#4716,#4717,#4718,#4719,#4720,#4721));
#5069=AXIS2_PLACEMENT_3D('',#7981,#5752,#5753);
#5070=AXIS2_PLACEMENT_3D('',#7982,#5754,#5755);
#5071=AXIS2_PLACEMENT_3D('',#8065,#5756,#5757);
#5072=AXIS2_PLACEMENT_3D('',#17516,#5758,#5759);
#5073=AXIS2_PLACEMENT_3D('',#24562,#5760,#5761);
#5074=AXIS2_PLACEMENT_3D('',#24615,#5762,#5763);
#5075=AXIS2_PLACEMENT_3D('',#46894,#5764,#5765);
#5076=AXIS2_PLACEMENT_3D('',#68909,#5766,#5767);
#5077=AXIS2_PLACEMENT_3D('',#68911,#5768,#5769);
#5078=AXIS2_PLACEMENT_3D('',#68924,#5776,#5777);
#5079=AXIS2_PLACEMENT_3D('',#68927,#5779,#5780);
#5080=AXIS2_PLACEMENT_3D('',#68928,#5781,#5782);
#5081=AXIS2_PLACEMENT_3D('',#68934,#5786,#5787);
#5082=AXIS2_PLACEMENT_3D('',#68938,#5790,#5791);
#5083=AXIS2_PLACEMENT_3D('',#68942,#5794,#5795);
#5084=AXIS2_PLACEMENT_3D('',#69037,#5796,#5797);
#5085=AXIS2_PLACEMENT_3D('',#69041,#5800,#5801);
#5086=AXIS2_PLACEMENT_3D('',#69045,#5804,#5805);
#5087=AXIS2_PLACEMENT_3D('',#69047,#5807,#5808);
#5088=AXIS2_PLACEMENT_3D('',#74492,#5809,#5810);
#5752=DIRECTION('axis',(0.,0.,1.));
#5753=DIRECTION('refdir',(1.,0.,0.));
#5754=DIRECTION('center_axis',(-1.,0.,0.));
#5755=DIRECTION('ref_axis',(0.,1.,0.));
#5756=DIRECTION('center_axis',(-1.,0.,0.));
#5757=DIRECTION('ref_axis',(0.,1.,0.));
#5758=DIRECTION('center_axis',(-1.,0.,0.));
#5759=DIRECTION('ref_axis',(0.,1.,0.));
#5760=DIRECTION('center_axis',(-1.,0.,0.));
#5761=DIRECTION('ref_axis',(0.,1.,2.00814192590157E-12));
#5762=DIRECTION('center_axis',(-1.,0.,0.));
#5763=DIRECTION('ref_axis',(0.,1.,2.00814192590157E-12));
#5764=DIRECTION('center_axis',(1.,0.,0.));
#5765=DIRECTION('ref_axis',(0.,1.,2.00814192590157E-12));
#5766=DIRECTION('center_axis',(1.,0.,0.));
#5767=DIRECTION('ref_axis',(0.,1.,0.));
#5768=DIRECTION('center_axis',(1.,0.,0.));
#5769=DIRECTION('ref_axis',(0.,1.,0.));
#5770=DIRECTION('',(0.,-0.5,0.866025403784439));
#5771=DIRECTION('',(0.,0.5,0.866025403784439));
#5772=DIRECTION('',(0.,1.,0.));
#5773=DIRECTION('',(0.,0.499999999999999,-0.866025403784439));
#5774=DIRECTION('',(0.,-0.500000000000001,-0.866025403784438));
#5775=DIRECTION('',(0.,-1.,0.));
#5776=DIRECTION('center_axis',(1.,0.,0.));
#5777=DIRECTION('ref_axis',(0.,1.,0.));
#5778=DIRECTION('',(-1.,0.,0.));
#5779=DIRECTION('center_axis',(1.,0.,0.));
#5780=DIRECTION('ref_axis',(0.,1.,0.));
#5781=DIRECTION('center_axis',(0.,-0.866025403784439,-0.499999999999999));
#5782=DIRECTION('ref_axis',(0.,0.499999999999999,-0.866025403784439));
#5783=DIRECTION('',(1.,0.,0.));
#5784=DIRECTION('',(0.,0.499999999999999,-0.866025403784439));
#5785=DIRECTION('',(1.,0.,0.));
#5786=DIRECTION('center_axis',(0.,0.,-1.));
#5787=DIRECTION('ref_axis',(0.,1.,0.));
#5788=DIRECTION('',(1.,0.,0.));
#5789=DIRECTION('',(0.,1.,0.));
#5790=DIRECTION('center_axis',(0.,0.866025403784439,-0.5));
#5791=DIRECTION('ref_axis',(0.,0.5,0.866025403784439));
#5792=DIRECTION('',(1.,0.,0.));
#5793=DIRECTION('',(0.,0.5,0.866025403784439));
#5794=DIRECTION('center_axis',(1.,0.,0.));
#5795=DIRECTION('ref_axis',(0.,1.,0.));
#5796=DIRECTION('center_axis',(0.,0.866025403784439,0.5));
#5797=DIRECTION('ref_axis',(0.,-0.5,0.866025403784439));
#5798=DIRECTION('',(1.,0.,0.));
#5799=DIRECTION('',(0.,-0.5,0.866025403784439));
#5800=DIRECTION('center_axis',(0.,-0.866025403784438,0.500000000000001));
#5801=DIRECTION('ref_axis',(0.,-0.500000000000001,-0.866025403784438));
#5802=DIRECTION('',(0.,-0.500000000000001,-0.866025403784438));
#5803=DIRECTION('',(1.,0.,0.));
#5804=DIRECTION('center_axis',(0.,0.,1.));
#5805=DIRECTION('ref_axis',(0.,-1.,0.));
#5806=DIRECTION('',(0.,-1.,0.));
#5807=DIRECTION('center_axis',(1.,0.,0.));
#5808=DIRECTION('ref_axis',(0.,0.,-1.));
#5809=DIRECTION('center_axis',(1.,0.,0.));
#5810=DIRECTION('ref_axis',(0.,1.,0.));
#7981=CARTESIAN_POINT('',(0.,0.,0.));
#7982=CARTESIAN_POINT('Origin',(185.231676812499,0.,335.));
#7983=CARTESIAN_POINT('',(184.668301620265,-5.91674928609117,334.997093448832));
#7984=CARTESIAN_POINT('',(185.231456596324,2.58392919827197,329.677290120548));
#7985=CARTESIAN_POINT('Ctrl Pts',(184.668301620294,-5.91674928609086,334.99709344821));
#7986=CARTESIAN_POINT('Ctrl Pts',(184.677270719926,-5.91665612605423,334.807451349904));
#7987=CARTESIAN_POINT('Ctrl Pts',(184.686239819557,-5.90744612029556,334.618059773088));
#7988=CARTESIAN_POINT('Ctrl Pts',(184.695208919188,-5.88918696321264,334.429555020334));
#7989=CARTESIAN_POINT('Ctrl Pts',(184.702645229547,-5.874048235298,334.273265102371));
#7990=CARTESIAN_POINT('Ctrl Pts',(184.710081539905,-5.85266154708832,334.117349686397));
#7991=CARTESIAN_POINT('Ctrl Pts',(184.717517850264,-5.82504996052314,333.962347110104));
#7992=CARTESIAN_POINT('Ctrl Pts',(184.724945525487,-5.7974704368756,333.80752452473));
#7993=CARTESIAN_POINT('Ctrl Pts',(184.732373200709,-5.76368046885996,333.653613031502));
#7994=CARTESIAN_POINT('Ctrl Pts',(184.739800875932,-5.72375497841269,333.501147268877));
#7995=CARTESIAN_POINT('Ctrl Pts',(184.747221528956,-5.68386723392797,333.348825648926));
#7996=CARTESIAN_POINT('Ctrl Pts',(184.754642181979,-5.63785560932689,333.197947395628));
#7997=CARTESIAN_POINT('Ctrl Pts',(184.762062835003,-5.58584629808054,333.049038263645));
#7998=CARTESIAN_POINT('Ctrl Pts',(184.769478073325,-5.53387493698251,332.900237787662));
#7999=CARTESIAN_POINT('Ctrl Pts',(184.776893311648,-5.47591472598483,332.753403921355));
#8000=CARTESIAN_POINT('Ctrl Pts',(184.78430854997,-5.41214201488629,332.609048437713));
#8001=CARTESIAN_POINT('Ctrl Pts',(184.791719976858,-5.34840208297505,332.46476715282));
#8002=CARTESIAN_POINT('Ctrl Pts',(184.799131403747,-5.27885575128642,332.322962052588));
#8003=CARTESIAN_POINT('Ctrl Pts',(184.806542830635,-5.20372789585258,332.184125970782));
#8004=CARTESIAN_POINT('Ctrl Pts',(184.813953122964,-5.12861154117879,332.04531114235));
#8005=CARTESIAN_POINT('Ctrl Pts',(184.821363415292,-5.0479155349489,331.909464757111));
#8006=CARTESIAN_POINT('Ctrl Pts',(184.828773707621,-4.96191127327889,331.777056147152));
#8007=CARTESIAN_POINT('Ctrl Pts',(184.836183730803,-4.87591013534358,331.644652346367));
#8008=CARTESIAN_POINT('Ctrl Pts',(184.843593753985,-4.78460132776732,331.515686384364));
#8009=CARTESIAN_POINT('Ctrl Pts',(184.851003777167,-4.68830011228147,331.390599409918));
#8010=CARTESIAN_POINT('Ctrl Pts',(184.858414979188,-4.59198357650121,331.265492535732));
#8011=CARTESIAN_POINT('Ctrl Pts',(184.86582618121,-4.49067327807438,331.14426617247));
#8012=CARTESIAN_POINT('Ctrl Pts',(184.873237383232,-4.38472528255571,331.027329014502));
#8013=CARTESIAN_POINT('Ctrl Pts',(184.880651212497,-4.27873972888114,330.910350402762));
#8014=CARTESIAN_POINT('Ctrl Pts',(184.888065041761,-4.16811345401209,330.79766429917));
#8015=CARTESIAN_POINT('Ctrl Pts',(184.895478871026,-4.05323984033218,330.689643012552));
#8016=CARTESIAN_POINT('Ctrl Pts',(184.902900803344,-3.93824067383906,330.581503662472));
#8017=CARTESIAN_POINT('Ctrl Pts',(184.910322735663,-3.81898516866113,330.478039566256));
#8018=CARTESIAN_POINT('Ctrl Pts',(184.917744667982,-3.69590085340995,330.379583628691));
#8019=CARTESIAN_POINT('Ctrl Pts',(184.92517116989,-3.57274075670458,330.281067073052));
#8020=CARTESIAN_POINT('Ctrl Pts',(184.932597671799,-3.44574745087061,330.187565040681));
#8021=CARTESIAN_POINT('Ctrl Pts',(184.940024173707,-3.31537756949373,330.099367170028));
#8022=CARTESIAN_POINT('Ctrl Pts',(184.947461126786,-3.18482422114322,330.011045180244));
#8023=CARTESIAN_POINT('Ctrl Pts',(184.954898079865,-3.05088512199134,329.928042455675));
#8024=CARTESIAN_POINT('Ctrl Pts',(184.962335032943,-2.91404232556548,329.850603153056));
#8025=CARTESIAN_POINT('Ctrl Pts',(184.96603900645,-2.84588778872343,329.812034518527));
#8026=CARTESIAN_POINT('Ctrl Pts',(184.969742979957,-2.77701331258672,329.774845169973));
#8027=CARTESIAN_POINT('Ctrl Pts',(184.973446953464,-2.70748021779954,329.739060784164));
#8028=CARTESIAN_POINT('Ctrl Pts',(184.98073525764,-2.57066003154614,329.668647891621));
#8029=CARTESIAN_POINT('Ctrl Pts',(184.988023561816,-2.43084361068165,329.603448846054));
#8030=CARTESIAN_POINT('Ctrl Pts',(184.995311865992,-2.28847483920939,329.543736308351));
#8031=CARTESIAN_POINT('Ctrl Pts',(185.002591396468,-2.14627745203645,329.484095652925));
#8032=CARTESIAN_POINT('Ctrl Pts',(185.009870926944,-2.00153417916713,329.429928515966));
#8033=CARTESIAN_POINT('Ctrl Pts',(185.01715045742,-1.85471492012095,329.381462545503));
#8034=CARTESIAN_POINT('Ctrl Pts',(185.02442294338,-1.70803774036211,329.333043476316));
#8035=CARTESIAN_POINT('Ctrl Pts',(185.031695429341,-1.55928893643624,329.290314718072));
#8036=CARTESIAN_POINT('Ctrl Pts',(185.038967915301,-1.40895960607995,329.253456396151));
#8037=CARTESIAN_POINT('Ctrl Pts',(185.04623507784,-1.25874031602008,329.216625054333));
#8038=CARTESIAN_POINT('Ctrl Pts',(185.053502240378,-1.10694317641211,329.185655689977));
#8039=CARTESIAN_POINT('Ctrl Pts',(185.060769402916,-0.954075423499419,329.160678922274));
#8040=CARTESIAN_POINT('Ctrl Pts',(185.06803359087,-0.801270242198636,329.135712378027));
#8041=CARTESIAN_POINT('Ctrl Pts',(185.075297778823,-0.647395700591261,329.116733615813));
#8042=CARTESIAN_POINT('Ctrl Pts',(185.082561966777,-0.492970065631674,329.103822333334));
#8043=CARTESIAN_POINT('Ctrl Pts',(185.089824724367,-0.338574838026922,329.090913593166));
#8044=CARTESIAN_POINT('Ctrl Pts',(185.097087481958,-0.18362911891612,329.084069989377));
#8045=CARTESIAN_POINT('Ctrl Pts',(185.104350239548,-0.0286568052247463,
329.083319397668));
#8046=CARTESIAN_POINT('Ctrl Pts',(185.111613114984,0.126318023040366,329.082568793779));
#8047=CARTESIAN_POINT('Ctrl Pts',(185.118875990419,0.2813190590681,329.08791140062));
#8048=CARTESIAN_POINT('Ctrl Pts',(185.126138865855,0.435822242651817,329.099322959583));
#8049=CARTESIAN_POINT('Ctrl Pts',(185.133403407354,0.590360868423202,329.110737136295));
#8050=CARTESIAN_POINT('Ctrl Pts',(185.140667948854,0.744401028100145,329.128223005766));
#8051=CARTESIAN_POINT('Ctrl Pts',(185.147932490353,0.897423966635176,329.151704454577));
#8052=CARTESIAN_POINT('Ctrl Pts',(185.155204498544,1.05060418625961,329.175210038254));
#8053=CARTESIAN_POINT('Ctrl Pts',(185.162476506734,1.20276471325446,329.204723448796));
#8054=CARTESIAN_POINT('Ctrl Pts',(185.169748514925,1.35339661489844,329.240117347959));
#8055=CARTESIAN_POINT('Ctrl Pts',(185.177024411585,1.50410906204926,329.275530172858));
#8056=CARTESIAN_POINT('Ctrl Pts',(185.184300308246,1.65329088351919,329.316829643947));
#8057=CARTESIAN_POINT('Ctrl Pts',(185.191576204906,1.80044935259379,329.363838833812));
#8058=CARTESIAN_POINT('Ctrl Pts',(185.198863103485,1.94783034071153,329.410919106504));
#8059=CARTESIAN_POINT('Ctrl Pts',(185.206150002065,2.09318150212912,329.463726209755));
#8060=CARTESIAN_POINT('Ctrl Pts',(185.213436900644,2.23603032721356,329.522035146308));
#8061=CARTESIAN_POINT('Ctrl Pts',(185.219443465871,2.35378011830126,329.570099000482));
#8062=CARTESIAN_POINT('Ctrl Pts',(185.225450031097,2.46982998827961,329.621900237034));
#8063=CARTESIAN_POINT('Ctrl Pts',(185.231456596324,2.58392919827197,329.677290120548));
#8064=CARTESIAN_POINT('',(185.231676812499,-2.58391981634259,329.677285566066));
#8065=CARTESIAN_POINT('Origin',(185.231676812499,0.,335.));
#8066=CARTESIAN_POINT('',(184.92005200467,-5.91674971498714,334.99816350889));
#8067=CARTESIAN_POINT('Ctrl Pts',(185.231676812499,-2.58391981634272,329.677285566066));
#8068=CARTESIAN_POINT('Ctrl Pts',(185.222990255087,-2.74992539420482,329.757873226288));
#8069=CARTESIAN_POINT('Ctrl Pts',(185.214303697674,-2.9120326743171,329.846169533597));
#8070=CARTESIAN_POINT('Ctrl Pts',(185.205617140262,-3.06960333180715,329.941792219782));
#8071=CARTESIAN_POINT('Ctrl Pts',(185.196915035362,-3.22745601446327,330.037586054608));
#8072=CARTESIAN_POINT('Ctrl Pts',(185.188212930462,-3.3807557423746,330.140732443059));
#8073=CARTESIAN_POINT('Ctrl Pts',(185.179510825562,-3.52889127698889,330.250804603126));
#8074=CARTESIAN_POINT('Ctrl Pts',(185.170808414404,-3.67703202502333,330.360880637026));
#8075=CARTESIAN_POINT('Ctrl Pts',(185.162106003246,-3.82000813672313,330.477882862259));
#8076=CARTESIAN_POINT('Ctrl Pts',(185.153403592088,-3.95723996846166,330.60134311471));
#8077=CARTESIAN_POINT('Ctrl Pts',(185.144712182513,-4.09429831178734,330.724647288771));
#8078=CARTESIAN_POINT('Ctrl Pts',(185.136020772939,-4.22562680319546,330.854393112017));
#8079=CARTESIAN_POINT('Ctrl Pts',(185.127329363365,-4.35068080432546,330.990073928191));
#8080=CARTESIAN_POINT('Ctrl Pts',(185.118669707585,-4.47527792455407,331.125259038726));
#8081=CARTESIAN_POINT('Ctrl Pts',(185.110010051805,-4.59364622847051,331.266335792731));
#8082=CARTESIAN_POINT('Ctrl Pts',(185.101350396025,-4.70528091083734,331.412764000988));
#8083=CARTESIAN_POINT('Ctrl Pts',(185.098419529137,-4.74306375144935,331.462322736108));
#8084=CARTESIAN_POINT('Ctrl Pts',(185.09548866225,-4.7800755565781,331.512494147303));
#8085=CARTESIAN_POINT('Ctrl Pts',(185.092557795362,-4.81629766947775,331.563256290981));
#8086=CARTESIAN_POINT('Ctrl Pts',(185.085133430901,-4.90805419681628,331.691845090786));
#8087=CARTESIAN_POINT('Ctrl Pts',(185.077709066439,-4.99468976033005,331.82415634738));
#8088=CARTESIAN_POINT('Ctrl Pts',(185.070284701978,-5.07589938186872,331.959740795977));
#8089=CARTESIAN_POINT('Ctrl Pts',(185.062861266599,-5.15709884087321,332.0953082776));
#8090=CARTESIAN_POINT('Ctrl Pts',(185.055437831219,-5.23287352017277,332.234147817386));
#8091=CARTESIAN_POINT('Ctrl Pts',(185.04801439584,-5.30296286537544,332.375782895615));
#8092=CARTESIAN_POINT('Ctrl Pts',(185.040590448726,-5.37305704218452,332.517427737452));
#8093=CARTESIAN_POINT('Ctrl Pts',(185.033166501612,-5.43746494147296,332.661868168696));
#8094=CARTESIAN_POINT('Ctrl Pts',(185.025742554498,-5.49597294178626,332.808605013775));
#8095=CARTESIAN_POINT('Ctrl Pts',(185.01831402987,-5.554517017412,332.955432334985));
#8096=CARTESIAN_POINT('Ctrl Pts',(185.010885505242,-5.60715379168083,333.104558553273));
#8097=CARTESIAN_POINT('Ctrl Pts',(185.003456980613,-5.65371843128783,333.255466118926));
#8098=CARTESIAN_POINT('Ctrl Pts',(184.996025702763,-5.70030032907097,333.406429615203));
#8099=CARTESIAN_POINT('Ctrl Pts',(184.988594424913,-5.74080550906829,333.559175417435));
#8100=CARTESIAN_POINT('Ctrl Pts',(184.981163147063,-5.77511970241285,333.713173288549));
#8101=CARTESIAN_POINT('Ctrl Pts',(184.973724976583,-5.8094657227244,333.86731399517));
#8102=CARTESIAN_POINT('Ctrl Pts',(184.966286806103,-5.8376092228219,334.022708725665));
#8103=CARTESIAN_POINT('Ctrl Pts',(184.958848635623,-5.85948739488292,334.178819123635));
#8104=CARTESIAN_POINT('Ctrl Pts',(184.957045349824,-5.86479146758363,334.216666019521));
#8105=CARTESIAN_POINT('Ctrl Pts',(184.955242064025,-5.86972753194538,334.254554963113));
#8106=CARTESIAN_POINT('Ctrl Pts',(184.953438778226,-5.874295153744,334.292478262384));
#8107=CARTESIAN_POINT('Ctrl Pts',(184.942309853718,-5.90248409539786,334.526520772377));
#8108=CARTESIAN_POINT('Ctrl Pts',(184.931180929211,-5.91667646850286,334.762180362099));
#8109=CARTESIAN_POINT('Ctrl Pts',(184.920052004703,-5.91674971498693,334.998163508196));
#8110=CARTESIAN_POINT('',(183.170052045876,-5.9141846117472,334.997236534231));
#8111=CARTESIAN_POINT('Ctrl Pts',(184.92005200467,-5.91674971498714,334.99816350889));
#8112=CARTESIAN_POINT('Ctrl Pts',(184.912619780223,-5.91679863113384,335.155760022943));
#8113=CARTESIAN_POINT('Ctrl Pts',(184.905187555776,-5.91054673781889,335.313517479779));
#8114=CARTESIAN_POINT('Ctrl Pts',(184.897755331329,-5.89798177210636,335.470894445074));
#8115=CARTESIAN_POINT('Ctrl Pts',(184.890328743703,-5.88542633603842,335.628152050986));
#8116=CARTESIAN_POINT('Ctrl Pts',(184.882902156077,-5.86656739122947,335.785029372013));
#8117=CARTESIAN_POINT('Ctrl Pts',(184.87547556845,-5.84144473319586,335.940985648944));
#8118=CARTESIAN_POINT('Ctrl Pts',(184.868053022074,-5.81633574590142,336.096857060747));
#8119=CARTESIAN_POINT('Ctrl Pts',(184.860630475698,-5.78496989265089,336.251808061564));
#8120=CARTESIAN_POINT('Ctrl Pts',(184.853207929321,-5.7474387245306,336.40530376441));
#8121=CARTESIAN_POINT('Ctrl Pts',(184.845786698478,-5.70991420823967,336.558772262476));
#8122=CARTESIAN_POINT('Ctrl Pts',(184.838365467636,-5.66622663380898,336.710785614705));
#8123=CARTESIAN_POINT('Ctrl Pts',(184.830944236793,-5.61651854641477,336.860819706548));
#8124=CARTESIAN_POINT('Ctrl Pts',(184.823523485506,-5.5668136711269,337.01084410328));
#8125=CARTESIAN_POINT('Ctrl Pts',(184.816102734218,-5.51108917306329,337.158889141963));
#8126=CARTESIAN_POINT('Ctrl Pts',(184.808681982931,-5.44953723355074,337.304446680365));
#8127=CARTESIAN_POINT('Ctrl Pts',(184.801260270523,-5.38797732195366,337.450023071088));
#8128=CARTESIAN_POINT('Ctrl Pts',(184.793838558114,-5.32058860997159,337.593110978218));
#8129=CARTESIAN_POINT('Ctrl Pts',(184.786416845706,-5.24761106128227,337.733223136154));
#8130=CARTESIAN_POINT('Ctrl Pts',(184.778992731212,-5.1746098929285,337.873380642313));
#8131=CARTESIAN_POINT('Ctrl Pts',(184.771568616717,-5.09601645692536,338.010560152565));
#8132=CARTESIAN_POINT('Ctrl Pts',(184.764144502223,-5.01211614933689,338.144299964707));
#8133=CARTESIAN_POINT('Ctrl Pts',(184.756711842999,-4.92811927731015,338.278193703696));
#8134=CARTESIAN_POINT('Ctrl Pts',(184.749279183775,-4.83880352864732,338.408639520922));
#8135=CARTESIAN_POINT('Ctrl Pts',(184.741846524551,-4.74449754696208,338.535204886477));
#8136=CARTESIAN_POINT('Ctrl Pts',(184.734409529676,-4.6501365543043,338.661844080688));
#8137=CARTESIAN_POINT('Ctrl Pts',(184.726972534801,-4.55077975997184,338.784598023861));
#8138=CARTESIAN_POINT('Ctrl Pts',(184.719535539926,-4.44679511124884,338.903068510938));
#8139=CARTESIAN_POINT('Ctrl Pts',(184.71208645424,-4.34264140785249,339.021731603267));
#8140=CARTESIAN_POINT('Ctrl Pts',(184.704637368554,-4.23384506932699,339.136097053411));
#8141=CARTESIAN_POINT('Ctrl Pts',(184.697188282868,-4.12081067877543,339.245803800482));
#8142=CARTESIAN_POINT('Ctrl Pts',(184.689859103229,-4.00959577420389,339.353744625809));
#8143=CARTESIAN_POINT('Ctrl Pts',(184.68252992359,-3.89427853114121,339.457175440066));
#8144=CARTESIAN_POINT('Ctrl Pts',(184.675200743952,-3.77527300229889,339.555792392176));
#8145=CARTESIAN_POINT('Ctrl Pts',(184.667838127936,-3.65572455952815,339.654859243694));
#8146=CARTESIAN_POINT('Ctrl Pts',(184.66047551192,-3.53206351088873,339.749391592085));
#8147=CARTESIAN_POINT('Ctrl Pts',(184.653112895905,-3.40467128147213,339.83902304475));
#8148=CARTESIAN_POINT('Ctrl Pts',(184.645759730408,-3.2774425703866,339.928539448124));
#8149=CARTESIAN_POINT('Ctrl Pts',(184.638406564911,-3.14649251509857,340.013167256584));
#8150=CARTESIAN_POINT('Ctrl Pts',(184.631053399415,-3.0122375759683,340.092578457758));
#8151=CARTESIAN_POINT('Ctrl Pts',(184.623708000047,-2.87812443171289,340.171905787893));
#8152=CARTESIAN_POINT('Ctrl Pts',(184.61636260068,-2.74071367435079,340.246027283195));
#8153=CARTESIAN_POINT('Ctrl Pts',(184.609017201312,-2.60045271628154,340.31465673707));
#8154=CARTESIAN_POINT('Ctrl Pts',(184.601677890707,-2.46030802359194,340.383229302488));
#8155=CARTESIAN_POINT('Ctrl Pts',(184.594338580102,-2.31731817234493,340.446318721519));
#8156=CARTESIAN_POINT('Ctrl Pts',(184.586999269496,-2.17195710676042,340.503683574561));
#8157=CARTESIAN_POINT('Ctrl Pts',(184.579664375719,-2.0266835200817,340.561013905191));
#8158=CARTESIAN_POINT('Ctrl Pts',(184.572329481942,-1.87904191250176,340.612626389189));
#8159=CARTESIAN_POINT('Ctrl Pts',(184.564994588165,-1.72952805167491,340.658326897677));
#8160=CARTESIAN_POINT('Ctrl Pts',(184.557661505516,-1.58005110871701,340.704016121823));
#8161=CARTESIAN_POINT('Ctrl Pts',(184.550328422866,-1.42870319402623,340.74379615947));
#8162=CARTESIAN_POINT('Ctrl Pts',(184.542995340217,-1.27599715176997,340.777522118623));
#8163=CARTESIAN_POINT('Ctrl Pts',(184.535662944991,-1.12330542461659,340.811244916207));
#8164=CARTESIAN_POINT('Ctrl Pts',(184.528330549766,-0.9692561943182,340.838914681973));
#8165=CARTESIAN_POINT('Ctrl Pts',(184.52099815454,-0.814374148435138,340.860437296726));
#8166=CARTESIAN_POINT('Ctrl Pts',(184.513664938763,-0.659474770038268,340.881962320029));
#8167=CARTESIAN_POINT('Ctrl Pts',(184.506331722985,-0.503742767188637,340.897338770723));
#8168=CARTESIAN_POINT('Ctrl Pts',(184.498998507207,-0.347709384272906,340.906524252603));
#8169=CARTESIAN_POINT('Ctrl Pts',(184.491662962579,-0.191626448962799,340.915712651569));
#8170=CARTESIAN_POINT('Ctrl Pts',(184.484327417951,-0.0352423224554345,
340.918706146454));
#8171=CARTESIAN_POINT('Ctrl Pts',(184.476991873322,0.120910551135107,340.915514449405));
#8172=CARTESIAN_POINT('Ctrl Pts',(184.469648295885,0.277234420369081,340.91231925728));
#8173=CARTESIAN_POINT('Ctrl Pts',(184.462304718448,0.433326150599635,340.902925355566));
#8174=CARTESIAN_POINT('Ctrl Pts',(184.454961141011,0.5886565605209,340.887394501497));
#8175=CARTESIAN_POINT('Ctrl Pts',(184.44761315717,0.744080174138074,340.871854328371));
#8176=CARTESIAN_POINT('Ctrl Pts',(184.440265173329,0.898741181947789,340.850169920815));
#8177=CARTESIAN_POINT('Ctrl Pts',(184.432917189488,1.05212010901704,340.822454279658));
#8178=CARTESIAN_POINT('Ctrl Pts',(184.425558330586,1.20572603784741,340.79469761918));
#8179=CARTESIAN_POINT('Ctrl Pts',(184.418199471683,1.35804572634777,340.760891980628));
#8180=CARTESIAN_POINT('Ctrl Pts',(184.41084061278,1.50857359387691,340.721200597284));
#8181=CARTESIAN_POINT('Ctrl Pts',(184.406214645079,1.60319927735646,340.696249574334));
#8182=CARTESIAN_POINT('Ctrl Pts',(184.401588677378,1.69711722968619,340.668973667477));
#8183=CARTESIAN_POINT('Ctrl Pts',(184.396962709677,1.79020608238217,340.639423086194));
#8184=CARTESIAN_POINT('Ctrl Pts',(184.38952595157,1.93985677705864,340.591917236793));
#8185=CARTESIAN_POINT('Ctrl Pts',(184.382089193462,2.08783569334246,340.538380481181));
#8186=CARTESIAN_POINT('Ctrl Pts',(184.374652435355,2.23362118212995,340.478947615851));
#8187=CARTESIAN_POINT('Ctrl Pts',(184.36722438968,2.37923587790224,340.41958437829));
#8188=CARTESIAN_POINT('Ctrl Pts',(184.359796344006,2.52266192055002,340.354338920509));
#8189=CARTESIAN_POINT('Ctrl Pts',(184.352368298332,2.66339208409924,340.283395988269));
#8190=CARTESIAN_POINT('Ctrl Pts',(184.344947351862,2.80398774764274,340.212520858301));
#8191=CARTESIAN_POINT('Ctrl Pts',(184.337526405392,2.94189233205641,340.135959261353));
#8192=CARTESIAN_POINT('Ctrl Pts',(184.330105458922,3.07661798277987,340.053944236983));
#8193=CARTESIAN_POINT('Ctrl Pts',(184.322690003926,3.21124393699783,339.971989903442));
#8194=CARTESIAN_POINT('Ctrl Pts',(184.315274548931,3.34269532561923,339.884590370821));
#8195=CARTESIAN_POINT('Ctrl Pts',(184.307859093935,3.47050841928556,339.792024819861));
#8196=CARTESIAN_POINT('Ctrl Pts',(184.300447526971,3.59825449867548,339.699507802375));
#8197=CARTESIAN_POINT('Ctrl Pts',(184.293035960007,3.72236578216018,339.601830378786));
#8198=CARTESIAN_POINT('Ctrl Pts',(184.285624393042,3.84240717485589,339.499315244025));
#8199=CARTESIAN_POINT('Ctrl Pts',(184.278214075443,3.96242833223092,339.396817390192));
#8200=CARTESIAN_POINT('Ctrl Pts',(184.270803757843,4.07838067841884,339.289483685316));
#8201=CARTESIAN_POINT('Ctrl Pts',(184.263393440243,4.18986180372311,339.177677420314));
#8202=CARTESIAN_POINT('Ctrl Pts',(184.255983463113,4.30133780698697,339.065876292291));
#8203=CARTESIAN_POINT('Ctrl Pts',(184.248573485983,4.40834273546606,338.949603276056));
#8204=CARTESIAN_POINT('Ctrl Pts',(184.241163508853,4.51051088298533,338.829258692877));
#8205=CARTESIAN_POINT('Ctrl Pts',(184.233752424211,4.6126943007808,338.708896122731));
#8206=CARTESIAN_POINT('Ctrl Pts',(184.22634133957,4.71003925753255,338.58446105728));
#8207=CARTESIAN_POINT('Ctrl Pts',(184.218930254928,4.80222029034206,338.456386964089));
#8208=CARTESIAN_POINT('Ctrl Pts',(184.211516614422,4.89443311367248,338.328268701919));
#8209=CARTESIAN_POINT('Ctrl Pts',(184.204102973916,4.9814782500839,338.19650921469));
#8210=CARTESIAN_POINT('Ctrl Pts',(184.196689333409,5.06307359867799,338.061570887121));
#8211=CARTESIAN_POINT('Ctrl Pts',(184.189267697252,5.14475694829225,337.926487027844));
#8212=CARTESIAN_POINT('Ctrl Pts',(184.181846061095,5.22097857950156,337.788217799716));
#8213=CARTESIAN_POINT('Ctrl Pts',(184.174424424938,5.29150204892088,337.647250768017));
#8214=CARTESIAN_POINT('Ctrl Pts',(184.166998280622,5.36206835673941,337.506198108058));
#8215=CARTESIAN_POINT('Ctrl Pts',(184.159572136306,5.42692945253008,337.362444716905));
#8216=CARTESIAN_POINT('Ctrl Pts',(184.152145991989,5.48589727294769,337.216497614067));
#8217=CARTESIAN_POINT('Ctrl Pts',(184.144709488946,5.54494734756367,337.070346929651));
#8218=CARTESIAN_POINT('Ctrl Pts',(184.137272985903,5.59808760342417,336.921996771054));
#8219=CARTESIAN_POINT('Ctrl Pts',(184.12983648286,5.64517975891654,336.771969540376));
#8220=CARTESIAN_POINT('Ctrl Pts',(184.126132547041,5.66863518151359,336.697244736216));
#8221=CARTESIAN_POINT('Ctrl Pts',(184.122428611222,5.69059099402034,336.622104058256));
#8222=CARTESIAN_POINT('Ctrl Pts',(184.118724675403,5.71103486732865,336.546612849635));
#8223=CARTESIAN_POINT('Ctrl Pts',(184.111291533105,5.75206209535312,336.395115382242));
#8224=CARTESIAN_POINT('Ctrl Pts',(184.103858390807,5.78711705717358,336.241762432013));
#8225=CARTESIAN_POINT('Ctrl Pts',(184.096425248508,5.81603124347139,336.087065378652));
#8226=CARTESIAN_POINT('Ctrl Pts',(184.089000704779,5.84491198218809,335.932547276973));
#8227=CARTESIAN_POINT('Ctrl Pts',(184.081576161049,5.8676660182781,335.776688529685));
#8228=CARTESIAN_POINT('Ctrl Pts',(184.07415161732,5.88417466538833,335.620015378601));
#8229=CARTESIAN_POINT('Ctrl Pts',(184.066734055716,5.90066778757921,335.463489564729));
#8230=CARTESIAN_POINT('Ctrl Pts',(184.059316494112,5.91092717525258,335.306151239589));
#8231=CARTESIAN_POINT('Ctrl Pts',(184.051898932508,5.91488524718123,335.148536443938));
#8232=CARTESIAN_POINT('Ctrl Pts',(184.044486742013,5.91884045304185,334.991035778282));
#8233=CARTESIAN_POINT('Ctrl Pts',(184.037074551518,5.91650341964218,334.833259411251));
#8234=CARTESIAN_POINT('Ctrl Pts',(184.029662361023,5.90785842858468,334.675748014191));
#8235=CARTESIAN_POINT('Ctrl Pts',(184.022253934834,5.89921782791392,334.518316609805));
#8236=CARTESIAN_POINT('Ctrl Pts',(184.014845508644,5.88427567030619,334.361150278058));
#8237=CARTESIAN_POINT('Ctrl Pts',(184.007437082454,5.86306832554752,334.204789101897));
#8238=CARTESIAN_POINT('Ctrl Pts',(184.000029708666,5.84186399339433,334.048450137594));
#8239=CARTESIAN_POINT('Ctrl Pts',(183.992622334879,5.81439628924412,333.892916470451));
#8240=CARTESIAN_POINT('Ctrl Pts',(183.985214961092,5.78075340524612,333.738722619629));
#8241=CARTESIAN_POINT('Ctrl Pts',(183.977807804681,5.74711150853291,333.584533293783));
#8242=CARTESIAN_POINT('Ctrl Pts',(183.970400648271,5.70729487142547,333.43168406971));
#8243=CARTESIAN_POINT('Ctrl Pts',(183.962993491861,5.6614426752963,333.280698573015));
#8244=CARTESIAN_POINT('Ctrl Pts',(183.955585101566,5.61558284110861,333.129687925157));
#8245=CARTESIAN_POINT('Ctrl Pts',(183.948176711272,5.56368555402802,332.980541978969));
#8246=CARTESIAN_POINT('Ctrl Pts',(183.940768320977,5.50593962476721,332.833768384748));
#8247=CARTESIAN_POINT('Ctrl Pts',(183.933357245087,5.44817276217845,332.686941584009));
#8248=CARTESIAN_POINT('Ctrl Pts',(183.925946169196,5.38455317201563,332.54248919366));
#8249=CARTESIAN_POINT('Ctrl Pts',(183.918535093305,5.31531741559422,332.400897975458));
#8250=CARTESIAN_POINT('Ctrl Pts',(183.911115809991,5.24600498378105,332.259149951542));
#8251=CARTESIAN_POINT('Ctrl Pts',(183.903696526677,5.17106412819874,332.120269762214));
#8252=CARTESIAN_POINT('Ctrl Pts',(183.896277243363,5.0907772599879,331.984719341141));
#8253=CARTESIAN_POINT('Ctrl Pts',(183.88885333492,5.01044034150579,331.849084418884));
#8254=CARTESIAN_POINT('Ctrl Pts',(183.881429426476,4.92475097110622,331.716783712901));
#8255=CARTESIAN_POINT('Ctrl Pts',(183.874005518033,4.83403404540267,331.58824892315));
#8256=CARTESIAN_POINT('Ctrl Pts',(183.866571048381,4.74318806632862,331.459531280555));
#8257=CARTESIAN_POINT('Ctrl Pts',(183.859136578729,4.64730047350111,331.334590548397));
#8258=CARTESIAN_POINT('Ctrl Pts',(183.851702109076,4.5467359840883,331.213824825302));
#8259=CARTESIAN_POINT('Ctrl Pts',(183.847963619761,4.49616623442231,331.153096705259));
#8260=CARTESIAN_POINT('Ctrl Pts',(183.844225130445,4.44441443244363,331.093423724049));
#8261=CARTESIAN_POINT('Ctrl Pts',(183.840486641129,4.39153029166857,331.03485280729));
#8262=CARTESIAN_POINT('Ctrl Pts',(183.833071341635,4.28663451446825,330.918677300895));
#8263=CARTESIAN_POINT('Ctrl Pts',(183.825656042141,4.17696364349042,330.806487844053));
#8264=CARTESIAN_POINT('Ctrl Pts',(183.818240742648,4.06285276260022,330.698702754757));
#8265=CARTESIAN_POINT('Ctrl Pts',(183.81083430635,3.94887827366561,330.591046496463));
#8266=CARTESIAN_POINT('Ctrl Pts',(183.803427870053,3.83047460714228,330.487784381869));
#8267=CARTESIAN_POINT('Ctrl Pts',(183.796021433756,3.70801650912296,330.389301123412));
#8268=CARTESIAN_POINT('Ctrl Pts',(183.788622225179,3.58567791431063,330.29091397183));
#8269=CARTESIAN_POINT('Ctrl Pts',(183.781223016603,3.45929305403203,330.197296625528));
#8270=CARTESIAN_POINT('Ctrl Pts',(183.773823808026,3.32927277795976,330.108796330919));
#8271=CARTESIAN_POINT('Ctrl Pts',(183.766430197456,3.1993508711017,330.020362992823));
#8272=CARTESIAN_POINT('Ctrl Pts',(183.759036586885,3.06579933267352,329.937039207934));
#8273=CARTESIAN_POINT('Ctrl Pts',(183.751642976315,2.92906117849915,329.859131282059));
#8274=CARTESIAN_POINT('Ctrl Pts',(183.744253338514,2.79239649710532,329.781265218032));
#8275=CARTESIAN_POINT('Ctrl Pts',(183.736863700713,2.65254893412756,329.708809402507));
#8276=CARTESIAN_POINT('Ctrl Pts',(183.729474062911,2.50998939743267,329.642026149068));
#8277=CARTESIAN_POINT('Ctrl Pts',(183.722085730066,2.36745503571489,329.575254689065));
#8278=CARTESIAN_POINT('Ctrl Pts',(183.714697397222,2.22220998950275,329.514153961201));
#8279=CARTESIAN_POINT('Ctrl Pts',(183.707309064377,2.07474870498796,329.458939778919));
#8280=CARTESIAN_POINT('Ctrl Pts',(183.699921103922,1.92729485287575,329.403728379564));
#8281=CARTESIAN_POINT('Ctrl Pts',(183.692533143466,1.77762533503827,329.354403067024));
#8282=CARTESIAN_POINT('Ctrl Pts',(183.685145183011,1.62625320201453,329.311130948472));
#8283=CARTESIAN_POINT('Ctrl Pts',(183.677756127613,1.47485863466583,329.267852416713));
#8284=CARTESIAN_POINT('Ctrl Pts',(183.670367072214,1.32176130954512,329.230628968008));
#8285=CARTESIAN_POINT('Ctrl Pts',(183.662978016816,1.1674878510558,329.199577370558));
#8286=CARTESIAN_POINT('Ctrl Pts',(183.655586398755,1.01316088765289,329.168515003836));
#8287=CARTESIAN_POINT('Ctrl Pts',(183.648194780694,0.857657345420576,329.143628823689));
#8288=CARTESIAN_POINT('Ctrl Pts',(183.640803162633,0.701512249812086,329.124984159522));
#8289=CARTESIAN_POINT('Ctrl Pts',(183.633403427034,0.545195674309636,329.106319019625));
#8290=CARTESIAN_POINT('Ctrl Pts',(183.626003691434,0.388236510204654,329.093909128754));
#8291=CARTESIAN_POINT('Ctrl Pts',(183.618603955834,0.231173818176808,329.087767830312));
#8292=CARTESIAN_POINT('Ctrl Pts',(183.611199675289,0.0740146576405804,329.081622759862));
#8293=CARTESIAN_POINT('Ctrl Pts',(183.603795394743,-0.0832477841853048,
329.081753953129));
#8294=CARTESIAN_POINT('Ctrl Pts',(183.596391114198,-0.240076805591269,329.088122659432));
#8295=CARTESIAN_POINT('Ctrl Pts',(183.588976229497,-0.397130432111038,329.094500486777));
#8296=CARTESIAN_POINT('Ctrl Pts',(183.581561344796,-0.553749026509288,329.107133638302));
#8297=CARTESIAN_POINT('Ctrl Pts',(183.574146460095,-0.709402527221167,329.12593168095));
#8298=CARTESIAN_POINT('Ctrl Pts',(183.570180509015,-0.792655901232077,329.135986067571));
#8299=CARTESIAN_POINT('Ctrl Pts',(183.566214557935,-0.875633368236423,329.147803228726));
#8300=CARTESIAN_POINT('Ctrl Pts',(183.562248606855,-0.958255423253487,329.1613634206));
#8301=CARTESIAN_POINT('Ctrl Pts',(183.554822205967,-1.11296850227204,329.186755418373));
#8302=CARTESIAN_POINT('Ctrl Pts',(183.547395805078,-1.26690385654412,329.218339191136));
#8303=CARTESIAN_POINT('Ctrl Pts',(183.539969404189,-1.41952706644195,329.256057671761));
#8304=CARTESIAN_POINT('Ctrl Pts',(183.532551750186,-1.57197051527248,329.2937317272));
#8305=CARTESIAN_POINT('Ctrl Pts',(183.525134096183,-1.72310453748313,329.337526019185));
#8306=CARTESIAN_POINT('Ctrl Pts',(183.517716442179,-1.87240167805583,329.387331960777));
#8307=CARTESIAN_POINT('Ctrl Pts',(183.510305911022,-2.02155545516595,329.437090075919));
#8308=CARTESIAN_POINT('Ctrl Pts',(183.502895379865,-2.16887551081852,329.492848230864));
#8309=CARTESIAN_POINT('Ctrl Pts',(183.495484848708,-2.31384650714532,329.55444723615));
#8310=CARTESIAN_POINT('Ctrl Pts',(183.488079821943,-2.45870982195383,329.616000486944));
#8311=CARTESIAN_POINT('Ctrl Pts',(183.480674795179,-2.60122720993012,329.683385804227));
#8312=CARTESIAN_POINT('Ctrl Pts',(183.473269768414,-2.74090048242339,329.756394836761));
#8313=CARTESIAN_POINT('Ctrl Pts',(183.465868631931,-2.88050037660378,329.829365513498));
#8314=CARTESIAN_POINT('Ctrl Pts',(183.458467495448,-3.01725880140435,329.907953849107));
#8315=CARTESIAN_POINT('Ctrl Pts',(183.451066358965,-3.15069957564894,329.991904279419));
#8316=CARTESIAN_POINT('Ctrl Pts',(183.44366644037,-3.28411839165312,330.075840895334));
#8317=CARTESIAN_POINT('Ctrl Pts',(183.436266521775,-3.41422032527419,330.165137656328));
#8318=CARTESIAN_POINT('Ctrl Pts',(183.42886660318,-3.54055564443255,330.259494089111));
#8319=CARTESIAN_POINT('Ctrl Pts',(183.42146700395,-3.6668855112183,330.353846449664));
#8320=CARTESIAN_POINT('Ctrl Pts',(183.414067404721,-3.78944878797824,330.453257824654));
#8321=CARTESIAN_POINT('Ctrl Pts',(183.406667805491,-3.90782670160056,330.55738578844));
#8322=CARTESIAN_POINT('Ctrl Pts',(183.399267068085,-4.02622282363367,330.661529768766));
#8323=CARTESIAN_POINT('Ctrl Pts',(183.391866330679,-4.14043202064027,330.770391536118));
#8324=CARTESIAN_POINT('Ctrl Pts',(183.384465593273,-4.25007055504534,330.883590054473));
#8325=CARTESIAN_POINT('Ctrl Pts',(183.377062259749,-4.35974754974122,330.996828281931));
#8326=CARTESIAN_POINT('Ctrl Pts',(183.369658926226,-4.46485043023356,331.114406021615));
#8327=CARTESIAN_POINT('Ctrl Pts',(183.362255592702,-4.56503420191328,331.2359073739));
#8328=CARTESIAN_POINT('Ctrl Pts',(183.354844149367,-4.6653277176057,331.357541822051));
#8329=CARTESIAN_POINT('Ctrl Pts',(183.347432706032,-4.76069112589044,331.48310817832));
#8330=CARTESIAN_POINT('Ctrl Pts',(183.340021262697,-4.85082098726279,331.612159048593));
#8331=CARTESIAN_POINT('Ctrl Pts',(183.332605261194,-4.94100628007502,331.741289287406));
#8332=CARTESIAN_POINT('Ctrl Pts',(183.325189259692,-5.02595141145103,331.873907997273));
#8333=CARTESIAN_POINT('Ctrl Pts',(183.31777325819,-5.10539803212959,332.009541590989));
#8334=CARTESIAN_POINT('Ctrl Pts',(183.310346732626,-5.18495739565542,332.14536766259));
#8335=CARTESIAN_POINT('Ctrl Pts',(183.302920207062,-5.25900248937629,332.284216834756));
#8336=CARTESIAN_POINT('Ctrl Pts',(183.295493681498,-5.32732202300773,332.425593150709));
#8337=CARTESIAN_POINT('Ctrl Pts',(183.291665978526,-5.36253457020601,332.498459868814));
#8338=CARTESIAN_POINT('Ctrl Pts',(183.287838275554,-5.3962269351572,332.571997616807));
#8339=CARTESIAN_POINT('Ctrl Pts',(183.284010572581,-5.42837534055216,332.646136850922));
#8340=CARTESIAN_POINT('Ctrl Pts',(183.275805271224,-5.4972906551283,332.805066308813));
#8341=CARTESIAN_POINT('Ctrl Pts',(183.267599969866,-5.55928544853722,332.967169333632));
#8342=CARTESIAN_POINT('Ctrl Pts',(183.259394668509,-5.61408642515934,333.131855419583));
#8343=CARTESIAN_POINT('Ctrl Pts',(183.251221118284,-5.66867534459627,333.295904238281));
#8344=CARTESIAN_POINT('Ctrl Pts',(183.24304756806,-5.71612589604507,333.462515953562));
#8345=CARTESIAN_POINT('Ctrl Pts',(183.234874017836,-5.75621375928746,333.631083012053));
#8346=CARTESIAN_POINT('Ctrl Pts',(183.226720710988,-5.79620233719068,333.799232581653));
#8347=CARTESIAN_POINT('Ctrl Pts',(183.21856740414,-5.82886453416691,333.969327605915));
#8348=CARTESIAN_POINT('Ctrl Pts',(183.210414097292,-5.85402514545746,334.140744415874));
#8349=CARTESIAN_POINT('Ctrl Pts',(183.202294040006,-5.87908315061312,334.311462180165));
#8350=CARTESIAN_POINT('Ctrl Pts',(183.19417398272,-5.89670053572695,334.48349074463));
#8351=CARTESIAN_POINT('Ctrl Pts',(183.186053925434,-5.90675291265045,334.656196871167));
#8352=CARTESIAN_POINT('Ctrl Pts',(183.180719971474,-5.9133561808052,334.769645150531));
#8353=CARTESIAN_POINT('Ctrl Pts',(183.175386017515,-5.91669614926623,334.883385452545));
#8354=CARTESIAN_POINT('Ctrl Pts',(183.170052063555,-5.91674935391449,334.997234958864));
#8355=CARTESIAN_POINT('',(181.420051985035,-5.91433197925221,335.005087499131));
#8356=CARTESIAN_POINT('Ctrl Pts',(183.170052004703,-5.90821144120066,334.997240203191));
#8357=CARTESIAN_POINT('Ctrl Pts',(183.115292182571,-5.90323267541164,336.164366188066));
#8358=CARTESIAN_POINT('Ctrl Pts',(182.967786349014,-5.00352060360718,339.315297141657));
#8359=CARTESIAN_POINT('Ctrl Pts',(182.727534504034,0.126099951212518,341.995542180405));
#8360=CARTESIAN_POINT('Ctrl Pts',(182.449296469759,5.95081939807114,338.679636353434));
#8361=CARTESIAN_POINT('Ctrl Pts',(182.171058435485,6.31467872490261,331.98709815247));
#8362=CARTESIAN_POINT('Ctrl Pts',(181.892820401213,0.883587563514807,328.059394286476));
#8363=CARTESIAN_POINT('Ctrl Pts',(181.642484924283,-4.73236743609919,330.256161176751));
#8364=CARTESIAN_POINT('Ctrl Pts',(181.484895458781,-5.90158033103822,333.625694798448));
#8365=CARTESIAN_POINT('Ctrl Pts',(181.420052004703,-5.91283370962365,335.005085791765));
#8366=CARTESIAN_POINT('',(179.670052004703,-5.92204575238021,335.000414748955));
#8367=CARTESIAN_POINT('Ctrl Pts',(181.420051953322,-5.91674781039664,335.005090252112));
#8368=CARTESIAN_POINT('Ctrl Pts',(181.411147422927,-5.91658474097863,335.194636978031));
#8369=CARTESIAN_POINT('Ctrl Pts',(181.402242892532,-5.90730958247142,335.383786698931));
#8370=CARTESIAN_POINT('Ctrl Pts',(181.393338362136,-5.88905914607669,335.571763007295));
#8371=CARTESIAN_POINT('Ctrl Pts',(181.384360339045,-5.87065808143897,335.761290760262));
#8372=CARTESIAN_POINT('Ctrl Pts',(181.375382315954,-5.84313306743074,335.949625655848));
#8373=CARTESIAN_POINT('Ctrl Pts',(181.366404292863,-5.80667280514391,336.1359936164));
#8374=CARTESIAN_POINT('Ctrl Pts',(181.357349481857,-5.76990070276834,336.323955558941));
#8375=CARTESIAN_POINT('Ctrl Pts',(181.348294670851,-5.7240398980615,336.509916787005));
#8376=CARTESIAN_POINT('Ctrl Pts',(181.339239859845,-5.66933204111301,336.693105067652));
#8377=CARTESIAN_POINT('Ctrl Pts',(181.338274684118,-5.66350058912769,336.712631580341));
#8378=CARTESIAN_POINT('Ctrl Pts',(181.337309508391,-5.65756866145798,336.732126607076));
#8379=CARTESIAN_POINT('Ctrl Pts',(181.336344332663,-5.65153658240612,336.751589227024));
#8380=CARTESIAN_POINT('Ctrl Pts',(181.328920381285,-5.60513895726375,336.901292063615));
#8381=CARTESIAN_POINT('Ctrl Pts',(181.321496429907,-5.55271903695615,337.049375946457));
#8382=CARTESIAN_POINT('Ctrl Pts',(181.314072478529,-5.49440646048727,337.19531961442));
#8383=CARTESIAN_POINT('Ctrl Pts',(181.306657288914,-5.43616270465071,337.341091039341));
#8384=CARTESIAN_POINT('Ctrl Pts',(181.2992420993,-5.37204027287378,337.484726933996));
#8385=CARTESIAN_POINT('Ctrl Pts',(181.291826909686,-5.30221888531639,337.625719987869));
#8386=CARTESIAN_POINT('Ctrl Pts',(181.284418855281,-5.23246468285505,337.766577372255));
#8387=CARTESIAN_POINT('Ctrl Pts',(181.277010800877,-5.15702260630546,337.904796646388));
#8388=CARTESIAN_POINT('Ctrl Pts',(181.269602746472,-5.07612084188826,338.039889432372));
#8389=CARTESIAN_POINT('Ctrl Pts',(181.262200206336,-4.9952792976128,338.174881660516));
#8390=CARTESIAN_POINT('Ctrl Pts',(181.2547976662,-4.90898634837258,338.30675171556));
#8391=CARTESIAN_POINT('Ctrl Pts',(181.247395126065,-4.81751652857495,338.435034942967));
#8392=CARTESIAN_POINT('Ctrl Pts',(181.23999648362,-4.72609487077569,338.563250624854));
#8393=CARTESIAN_POINT('Ctrl Pts',(181.232597841176,-4.62950198713847,338.687882937227));
#8394=CARTESIAN_POINT('Ctrl Pts',(181.225199198731,-4.5280561621734,338.80849549753));
#8395=CARTESIAN_POINT('Ctrl Pts',(181.217801777159,-4.42662707707912,338.929088155203));
#8396=CARTESIAN_POINT('Ctrl Pts',(181.210404355586,-4.32034687998087,339.045662091926));
#8397=CARTESIAN_POINT('Ctrl Pts',(181.203006934013,-4.20957471251635,339.157813283716));
#8398=CARTESIAN_POINT('Ctrl Pts',(181.195609833377,-4.09880735090034,339.269959609828));
#8399=CARTESIAN_POINT('Ctrl Pts',(181.188212732741,-3.98354866867682,339.377683307001));
#8400=CARTESIAN_POINT('Ctrl Pts',(181.180815632105,-3.8641951145148,339.480616774447));
#8401=CARTESIAN_POINT('Ctrl Pts',(181.173417392669,-3.74482318560877,339.583566088729));
#8402=CARTESIAN_POINT('Ctrl Pts',(181.166019153234,-3.62135541216968,339.681723461133));
#8403=CARTESIAN_POINT('Ctrl Pts',(181.158620913798,-3.4942216771828,339.77476129594));
#8404=CARTESIAN_POINT('Ctrl Pts',(181.151220075422,-3.36704328118306,339.867831814156));
#8405=CARTESIAN_POINT('Ctrl Pts',(181.143819237047,-3.23619666057628,339.955778993795));
#8406=CARTESIAN_POINT('Ctrl Pts',(181.136418398672,-3.10214090914292,340.038318404222));
#8407=CARTESIAN_POINT('Ctrl Pts',(181.129009433525,-2.9679379526995,340.120948450184));
#8408=CARTESIAN_POINT('Ctrl Pts',(181.121600468378,-2.83051914599176,340.198158672226));
#8409=CARTESIAN_POINT('Ctrl Pts',(181.114191503231,-2.69036906890002,340.269710128233));
#8410=CARTESIAN_POINT('Ctrl Pts',(181.106777973981,-2.55013265593105,340.341305661689));
#8411=CARTESIAN_POINT('Ctrl Pts',(181.09936444473,-2.40716195803917,340.407235326995));
#8412=CARTESIAN_POINT('Ctrl Pts',(181.091950915479,-2.26196129838316,340.467308446312));
#8413=CARTESIAN_POINT('Ctrl Pts',(181.084526831572,-2.11655391626657,340.527467091846));
#8414=CARTESIAN_POINT('Ctrl Pts',(181.077102747665,-1.96891058101614,340.581752410341));
#8415=CARTESIAN_POINT('Ctrl Pts',(181.069678663759,-1.81955130189638,340.630023412231));
#8416=CARTESIAN_POINT('Ctrl Pts',(181.065821208636,-1.74194620966027,340.655104381931));
#8417=CARTESIAN_POINT('Ctrl Pts',(181.061963753514,-1.66387805203984,340.678562502924));
#8418=CARTESIAN_POINT('Ctrl Pts',(181.058106298391,-1.58542071034248,340.700383472515));
#8419=CARTESIAN_POINT('Ctrl Pts',(181.050682308358,-1.43442309553192,340.742379725378));
#8420=CARTESIAN_POINT('Ctrl Pts',(181.043258318325,-1.28152788807992,340.778435516522));
#8421=CARTESIAN_POINT('Ctrl Pts',(181.035834328293,-1.12724358945137,340.808377781493));
#8422=CARTESIAN_POINT('Ctrl Pts',(181.028419099551,-0.973141366712676,340.838284710628));
#8423=CARTESIAN_POINT('Ctrl Pts',(181.021003870809,-0.81765367868449,340.862092404294));
#8424=CARTESIAN_POINT('Ctrl Pts',(181.013588642066,-0.661304396650291,340.879677462027));
#8425=CARTESIAN_POINT('Ctrl Pts',(181.006180548101,-0.505105550602682,340.897245599788));
#8426=CARTESIAN_POINT('Ctrl Pts',(180.998772454136,-0.348047129341617,340.90860297976));
#8427=CARTESIAN_POINT('Ctrl Pts',(180.991364360171,-0.190663310515679,340.913677203274));
#8428=CARTESIAN_POINT('Ctrl Pts',(180.983961780082,-0.0333966331472128,
340.918747650022));
#8429=CARTESIAN_POINT('Ctrl Pts',(180.976559199994,0.12419458812263,340.91754424009));
#8430=CARTESIAN_POINT('Ctrl Pts',(180.969156619905,0.281571043968763,340.910046388117));
#8431=CARTESIAN_POINT('Ctrl Pts',(180.961757937154,0.438864643663797,340.902552483642));
#8432=CARTESIAN_POINT('Ctrl Pts',(180.954359254404,0.59594333127363,340.888770754714));
#8433=CARTESIAN_POINT('Ctrl Pts',(180.946960571654,0.752267896746034,340.868732705962));
#8434=CARTESIAN_POINT('Ctrl Pts',(180.939563109374,0.908566675243656,340.848697962644));
#8435=CARTESIAN_POINT('Ctrl Pts',(180.932165647095,1.06411120867336,340.822408995151));
#8436=CARTESIAN_POINT('Ctrl Pts',(180.924768184816,1.2183673882307,340.789949176789));
#8437=CARTESIAN_POINT('Ctrl Pts',(180.91737104323,1.37261688052187,340.757490765614));
#8438=CARTESIAN_POINT('Ctrl Pts',(180.909973901643,1.52557776478184,340.718862112333));
#8439=CARTESIAN_POINT('Ctrl Pts',(180.902576760056,1.67672637260299,340.674197673144));
#8440=CARTESIAN_POINT('Ctrl Pts',(180.89517847946,1.82789825424608,340.629526356538));
#8441=CARTESIAN_POINT('Ctrl Pts',(180.887780198863,1.97725694588523,340.578817509257));
#8442=CARTESIAN_POINT('Ctrl Pts',(180.880381918267,2.12429432726241,340.522255352088));
#8443=CARTESIAN_POINT('Ctrl Pts',(180.872981038556,2.27138336483281,340.465673323878));
#8444=CARTESIAN_POINT('Ctrl Pts',(180.865580158844,2.41614912036067,340.403234025507));
#8445=CARTESIAN_POINT('Ctrl Pts',(180.858179279133,2.55810396458789,340.335169600759));
#8446=CARTESIAN_POINT('Ctrl Pts',(180.850770272591,2.70021468799824,340.267030435152));
#8447=CARTESIAN_POINT('Ctrl Pts',(180.843361266048,2.8395079992099,340.193253969033));
#8448=CARTESIAN_POINT('Ctrl Pts',(180.835952259506,2.97552072938724,340.114118394356));
#8449=CARTESIAN_POINT('Ctrl Pts',(180.828538688764,3.11161724802215,340.034934069479));
#8450=CARTESIAN_POINT('Ctrl Pts',(180.821125118022,3.24442884452244,339.950384257538));
#8451=CARTESIAN_POINT('Ctrl Pts',(180.81371154728,3.37352225236713,339.860789871542));
#8452=CARTESIAN_POINT('Ctrl Pts',(180.806287422088,3.50279944612216,339.771067933054));
#8453=CARTESIAN_POINT('Ctrl Pts',(180.798863296897,3.62834758206704,339.6762873013));
#8454=CARTESIAN_POINT('Ctrl Pts',(180.791439171705,3.74976668902281,339.576808969183));
#8455=CARTESIAN_POINT('Ctrl Pts',(180.787582202509,3.81284614192855,339.525128151203));
#8456=CARTESIAN_POINT('Ctrl Pts',(180.783725233312,3.87481177557784,339.472180039224));
#8457=CARTESIAN_POINT('Ctrl Pts',(180.779868264116,3.93561160099101,339.418019000485));
#8458=CARTESIAN_POINT('Ctrl Pts',(180.772444286588,4.05264041677785,339.313768664529));
#8459=CARTESIAN_POINT('Ctrl Pts',(180.76502030906,4.16570068763168,339.20470789023));
#8460=CARTESIAN_POINT('Ctrl Pts',(180.757596331532,4.2743717010055,339.091170630045));
#8461=CARTESIAN_POINT('Ctrl Pts',(180.750181115384,4.38291446668223,338.97776736044));
#8462=CARTESIAN_POINT('Ctrl Pts',(180.742765899235,4.4870780301344,338.859898387656));
#8463=CARTESIAN_POINT('Ctrl Pts',(180.735350683087,4.58647512470673,338.737937465093));
#8464=CARTESIAN_POINT('Ctrl Pts',(180.727942601792,4.68577658030326,338.616093892215));
#8465=CARTESIAN_POINT('Ctrl Pts',(180.720534520497,4.78032046319195,338.490166495232));
#8466=CARTESIAN_POINT('Ctrl Pts',(180.713126439202,4.86975681774697,338.360565294486));
#8467=CARTESIAN_POINT('Ctrl Pts',(180.705723871847,4.95912660355486,338.231060557753));
#8468=CARTESIAN_POINT('Ctrl Pts',(180.698321304492,5.04339621951318,338.097887767828));
#8469=CARTESIAN_POINT('Ctrl Pts',(180.690918737137,5.12225650378825,337.961489299643));
#8470=CARTESIAN_POINT('Ctrl Pts',(180.683520067171,5.20107526878811,337.825162644102));
#8471=CARTESIAN_POINT('Ctrl Pts',(180.676121397205,5.27449018766949,337.685614014833));
#8472=CARTESIAN_POINT('Ctrl Pts',(180.668722727239,5.34223595584715,337.543313892258));
#8473=CARTESIAN_POINT('Ctrl Pts',(180.66132527778,5.4099705484838,337.40103724393));
#8474=CARTESIAN_POINT('Ctrl Pts',(180.653927828321,5.47203768621696,337.256010339773));
#8475=CARTESIAN_POINT('Ctrl Pts',(180.646530378861,5.52821844247713,337.108727439655));
#8476=CARTESIAN_POINT('Ctrl Pts',(180.639133250115,5.5843967630473,336.961450924918));
#8477=CARTESIAN_POINT('Ctrl Pts',(180.631736121368,5.63468907655627,336.811918957398));
#8478=CARTESIAN_POINT('Ctrl Pts',(180.624338992622,5.67892506300316,336.660644661357));
#8479=CARTESIAN_POINT('Ctrl Pts',(180.616940724875,5.72316786085186,336.50934707229));
#8480=CARTESIAN_POINT('Ctrl Pts',(180.609542457128,5.76135237006233,336.356306978751));
#8481=CARTESIAN_POINT('Ctrl Pts',(180.60214418938,5.79335853271784,336.202051360752));
#8482=CARTESIAN_POINT('Ctrl Pts',(180.594743322517,5.82537593959296,336.047741550562));
#8483=CARTESIAN_POINT('Ctrl Pts',(180.587342455653,5.85121060259573,335.892215730893));
#8484=CARTESIAN_POINT('Ctrl Pts',(180.579941588789,5.87079385213348,335.736009584348));
#8485=CARTESIAN_POINT('Ctrl Pts',(180.572532595026,5.89039860605714,335.579631907677));
#8486=CARTESIAN_POINT('Ctrl Pts',(180.565123601263,5.90373819092342,335.422572782731));
#8487=CARTESIAN_POINT('Ctrl Pts',(180.557714607501,5.91079589696642,335.265372242152));
#8488=CARTESIAN_POINT('Ctrl Pts',(180.550301049519,5.91785795082189,335.108074860126));
#8489=CARTESIAN_POINT('Ctrl Pts',(180.542887491537,5.91863041279232,334.950636261208));
#8490=CARTESIAN_POINT('Ctrl Pts',(180.535473933555,5.91314868001698,334.79359445135));
#8491=CARTESIAN_POINT('Ctrl Pts',(180.528049820983,5.9076591429672,334.63632906303));
#8492=CARTESIAN_POINT('Ctrl Pts',(180.520625708411,5.89589765589368,334.479461963158));
#8493=CARTESIAN_POINT('Ctrl Pts',(180.51320159584,5.87795133799407,334.323524848443));
#8494=CARTESIAN_POINT('Ctrl Pts',(180.509344473841,5.86862751148914,334.242509310247));
#8495=CARTESIAN_POINT('Ctrl Pts',(180.505487351842,5.85763510645131,334.16174461945));
#8496=CARTESIAN_POINT('Ctrl Pts',(180.501630229842,5.8449917094733,334.081303924745));
#8497=CARTESIAN_POINT('Ctrl Pts',(180.494206255989,5.82065640231641,333.926476150457));
#8498=CARTESIAN_POINT('Ctrl Pts',(180.486782282135,5.79012829443469,333.772382401797));
#8499=CARTESIAN_POINT('Ctrl Pts',(180.479358308281,5.75346054108848,333.619557185307));
#8500=CARTESIAN_POINT('Ctrl Pts',(180.471943095889,5.71683606148139,333.466912326705));
#8501=CARTESIAN_POINT('Ctrl Pts',(180.464527883496,5.6740864454201,333.315533379716));
#8502=CARTESIAN_POINT('Ctrl Pts',(180.457112671104,5.62531641712912,333.165948264176));
#8503=CARTESIAN_POINT('Ctrl Pts',(180.449704593642,5.57659331544779,333.016507079706));
#8504=CARTESIAN_POINT('Ctrl Pts',(180.442296516181,5.52186144893766,332.868856642942));
#8505=CARTESIAN_POINT('Ctrl Pts',(180.434888438719,5.46127623062284,332.723513124278));
#8506=CARTESIAN_POINT('Ctrl Pts',(180.427485875272,5.40073610737101,332.578277788358));
#8507=CARTESIAN_POINT('Ctrl Pts',(180.420083311824,5.33435145030333,332.435346294556));
#8508=CARTESIAN_POINT('Ctrl Pts',(180.412680748376,5.2623269559899,332.295218017887));
#8509=CARTESIAN_POINT('Ctrl Pts',(180.405282082387,5.19034038266485,332.155163518936));
#8510=CARTESIAN_POINT('Ctrl Pts',(180.397883416398,5.11272005597363,332.017909628877));
#8511=CARTESIAN_POINT('Ctrl Pts',(180.390484750409,5.02971804069313,331.883934051785));
#8512=CARTESIAN_POINT('Ctrl Pts',(180.383087305019,4.94672971871036,331.749980577378));
#8513=CARTESIAN_POINT('Ctrl Pts',(180.375689859629,4.85836166658881,331.619304659494));
#8514=CARTESIAN_POINT('Ctrl Pts',(180.368292414238,4.76491104358145,331.492357870413));
#8515=CARTESIAN_POINT('Ctrl Pts',(180.360895289618,4.67146447280226,331.365416586028));
#8516=CARTESIAN_POINT('Ctrl Pts',(180.353498164997,4.57293599060056,331.242204409484));
#8517=CARTESIAN_POINT('Ctrl Pts',(180.346101040377,4.46966492353788,331.123142247413));
#8518=CARTESIAN_POINT('Ctrl Pts',(180.338702776809,4.36637795566442,331.004061753151));
#8519=CARTESIAN_POINT('Ctrl Pts',(180.331304513242,4.25834719351518,330.889132827614));
#8520=CARTESIAN_POINT('Ctrl Pts',(180.323906249674,4.14595081497659,330.778741609153));
#8521=CARTESIAN_POINT('Ctrl Pts',(180.31650538704,4.03351495073477,330.668311609417));
#8522=CARTESIAN_POINT('Ctrl Pts',(180.309104524407,3.916710682658,330.56242275202));
#8523=CARTESIAN_POINT('Ctrl Pts',(180.301703661773,3.79595131603305,330.461422671276));
#8524=CARTESIAN_POINT('Ctrl Pts',(180.294294672295,3.67505934425942,330.360311682939));
#8525=CARTESIAN_POINT('Ctrl Pts',(180.286885682818,3.55020388704537,330.264100431691));
#8526=CARTESIAN_POINT('Ctrl Pts',(180.27947669334,3.42183002618858,330.173095211797));
#8527=CARTESIAN_POINT('Ctrl Pts',(180.272063139682,3.29337708281574,330.082033929698));
#8528=CARTESIAN_POINT('Ctrl Pts',(180.264649586023,3.16140172898108,329.996185272524));
#8529=CARTESIAN_POINT('Ctrl Pts',(180.257236032365,3.02637554025923,329.915810619989));
#8530=CARTESIAN_POINT('Ctrl Pts',(180.249811924139,2.89115711673847,329.835321539243));
#8531=CARTESIAN_POINT('Ctrl Pts',(180.242387815914,2.75287951081335,329.76032220529));
#8532=CARTESIAN_POINT('Ctrl Pts',(180.234963707688,2.61203698228368,329.691027089381));
#8533=CARTESIAN_POINT('Ctrl Pts',(180.231106536981,2.53886271559002,329.655025042663));
#8534=CARTESIAN_POINT('Ctrl Pts',(180.227249366275,2.46499640991772,329.62056192608));
#8535=CARTESIAN_POINT('Ctrl Pts',(180.223392195568,2.39050909743196,329.587662536612));
#8536=CARTESIAN_POINT('Ctrl Pts',(180.215968216101,2.24714176408294,329.52434037369));
#8537=CARTESIAN_POINT('Ctrl Pts',(180.208544236634,2.10104040776048,329.466623103546));
#8538=CARTESIAN_POINT('Ctrl Pts',(180.201120257167,1.95268327283604,329.41475527855));
#8539=CARTESIAN_POINT('Ctrl Pts',(180.193705039089,1.80450122119061,329.36294866523));
#8540=CARTESIAN_POINT('Ctrl Pts',(180.186289821012,1.65406903887216,329.316977878085));
#8541=CARTESIAN_POINT('Ctrl Pts',(180.178874602934,1.5018873381933,329.277040539557));
#8542=CARTESIAN_POINT('Ctrl Pts',(180.171466519721,1.34985206555842,329.237141628424));
#8543=CARTESIAN_POINT('Ctrl Pts',(180.164058436509,1.19607098441952,329.203264702665));
#8544=CARTESIAN_POINT('Ctrl Pts',(180.156650353296,1.04106225727171,329.175558401101));
#8545=CARTESIAN_POINT('Ctrl Pts',(180.149247784037,0.886168905573019,329.147872721776));
#8546=CARTESIAN_POINT('Ctrl Pts',(180.141845214778,0.730050093102275,329.126348586912));
#8547=CARTESIAN_POINT('Ctrl Pts',(180.134442645519,0.573236528843565,329.111084102783));
#8548=CARTESIAN_POINT('Ctrl Pts',(180.127043973665,0.416505525911596,329.095827655306));
#8549=CARTESIAN_POINT('Ctrl Pts',(180.119645301811,0.259080870188701,329.086824331117));
#8550=CARTESIAN_POINT('Ctrl Pts',(180.112246629957,0.101500680689412,329.084120676153));
#8551=CARTESIAN_POINT('Ctrl Pts',(180.104849178638,-0.0560535132966765,
329.081417467203));
#8552=CARTESIAN_POINT('Ctrl Pts',(180.09745172732,-0.213762817343169,329.085011871325));
#8553=CARTESIAN_POINT('Ctrl Pts',(180.090054276002,-0.371086684064145,329.094898372135));
#8554=CARTESIAN_POINT('Ctrl Pts',(180.082657145415,-0.52840372969085,329.104784444296));
#8555=CARTESIAN_POINT('Ctrl Pts',(180.075260014828,-0.685334998743519,329.120962047307));
#8556=CARTESIAN_POINT('Ctrl Pts',(180.067862884241,-0.841342912134583,329.143373610456));
#8557=CARTESIAN_POINT('Ctrl Pts',(180.060464614674,-0.997374846995422,329.165788624447));
#8558=CARTESIAN_POINT('Ctrl Pts',(180.053066345106,-1.15248277366524,329.194439456751));
#8559=CARTESIAN_POINT('Ctrl Pts',(180.045668075539,-1.30613732580632,329.229217050639));
#8560=CARTESIAN_POINT('Ctrl Pts',(180.038267206877,-1.45984585850437,329.264006862284));
#8561=CARTESIAN_POINT('Ctrl Pts',(180.030866338216,-1.61209963632193,329.304927638603));
#8562=CARTESIAN_POINT('Ctrl Pts',(180.023465469554,-1.76238266236629,329.351819946754));
#8563=CARTESIAN_POINT('Ctrl Pts',(180.016056474035,-1.91283071344254,329.398763747111));
#8564=CARTESIAN_POINT('Ctrl Pts',(180.008647478517,-2.06130333449412,329.451692063365));
#8565=CARTESIAN_POINT('Ctrl Pts',(180.001238482999,-2.20730209629018,329.510396369663));
#8566=CARTESIAN_POINT('Ctrl Pts',(179.993824923283,-2.35339079836859,329.569136839842));
#8567=CARTESIAN_POINT('Ctrl Pts',(179.986411363568,-2.49700226482026,329.633660237673));
#8568=CARTESIAN_POINT('Ctrl Pts',(179.978997803852,-2.63766149872952,329.703711452289));
#8569=CARTESIAN_POINT('Ctrl Pts',(179.971573689596,-2.77852098645556,329.773862397457));
#8570=CARTESIAN_POINT('Ctrl Pts',(179.964149575339,-2.91641952105426,329.849556697965));
#8571=CARTESIAN_POINT('Ctrl Pts',(179.956725461083,-3.05090927621345,329.930494782445));
#8572=CARTESIAN_POINT('Ctrl Pts',(179.952868361153,-3.12078164175435,329.972545088941));
#8573=CARTESIAN_POINT('Ctrl Pts',(179.949011261224,-3.18973442331561,330.016010096609));
#8574=CARTESIAN_POINT('Ctrl Pts',(179.945154161294,-3.25770833231832,330.06084349468));
#8575=CARTESIAN_POINT('Ctrl Pts',(179.937744834982,-3.38828334508317,330.14696656177));
#8576=CARTESIAN_POINT('Ctrl Pts',(179.93033550867,-3.51564163243029,330.238403655687));
#8577=CARTESIAN_POINT('Ctrl Pts',(179.922926182357,-3.63931980341617,330.334886718314));
#8578=CARTESIAN_POINT('Ctrl Pts',(179.915525610116,-3.7628518494352,330.431255786821));
#8579=CARTESIAN_POINT('Ctrl Pts',(179.908125037876,-3.88271214065072,330.532658729572));
#8580=CARTESIAN_POINT('Ctrl Pts',(179.900724465635,-3.99846455809472,330.638783227107));
#8581=CARTESIAN_POINT('Ctrl Pts',(179.893331006724,-4.11410571587917,330.744805719209));
#8582=CARTESIAN_POINT('Ctrl Pts',(179.885937547813,-4.22564658549171,330.855540480191));
#8583=CARTESIAN_POINT('Ctrl Pts',(179.878544088903,-4.33268267761745,330.970633873973));
#8584=CARTESIAN_POINT('Ctrl Pts',(179.871156108305,-4.43963945947479,331.085641987287));
#8585=CARTESIAN_POINT('Ctrl Pts',(179.863768127707,-4.54209785545166,331.205002029864));
#8586=CARTESIAN_POINT('Ctrl Pts',(179.856380147109,-4.63968903768038,331.328322427537));
#8587=CARTESIAN_POINT('Ctrl Pts',(179.848616474509,-4.7422429057455,331.457913887583));
#8588=CARTESIAN_POINT('Ctrl Pts',(179.840852801909,-4.83942128334582,331.591878732752));
#8589=CARTESIAN_POINT('Ctrl Pts',(179.833089129308,-4.9308424271595,331.729721186042));
#8590=CARTESIAN_POINT('Ctrl Pts',(179.825706198374,-5.01778014665303,331.860803647259));
#8591=CARTESIAN_POINT('Ctrl Pts',(179.818323267439,-5.099511607423,331.99539212213));
#8592=CARTESIAN_POINT('Ctrl Pts',(179.810940336504,-5.17575203052851,332.133029215185));
#8593=CARTESIAN_POINT('Ctrl Pts',(179.803557579899,-5.25199065340122,332.270663058275));
#8594=CARTESIAN_POINT('Ctrl Pts',(179.796174823294,-5.32273831456115,332.411345048581));
#8595=CARTESIAN_POINT('Ctrl Pts',(179.788792066689,-5.38775575268492,332.554592362834));
#8596=CARTESIAN_POINT('Ctrl Pts',(179.781408012026,-5.45278462237157,332.697864863263));
#8597=CARTESIAN_POINT('Ctrl Pts',(179.774023957363,-5.51208110828031,332.843703244236));
#8598=CARTESIAN_POINT('Ctrl Pts',(179.766639902699,-5.56545380867749,332.991604006682));
#8599=CARTESIAN_POINT('Ctrl Pts',(179.759253077072,-5.61884653788094,333.13956027083));
#8600=CARTESIAN_POINT('Ctrl Pts',(179.751866251445,-5.66631092890013,333.289580104872));
#8601=CARTESIAN_POINT('Ctrl Pts',(179.744479425819,-5.70770527279833,333.441144303866));
#8602=CARTESIAN_POINT('Ctrl Pts',(179.737084455399,-5.74914525854128,333.592875619161));
#8603=CARTESIAN_POINT('Ctrl Pts',(179.729689484979,-5.7845017345088,333.746154337788));
#8604=CARTESIAN_POINT('Ctrl Pts',(179.72229451456,-5.81368385881868,333.900449840975));
#8605=CARTESIAN_POINT('Ctrl Pts',(179.714894800955,-5.84288470074761,334.05484431038));
#8606=CARTESIAN_POINT('Ctrl Pts',(179.707495087349,-5.86590324605129,334.210256493988));
#8607=CARTESIAN_POINT('Ctrl Pts',(179.700095373744,-5.8827005326052,334.366150643933));
#8608=CARTESIAN_POINT('Ctrl Pts',(179.692685469894,-5.89952095092716,334.522259477797));
#8609=CARTESIAN_POINT('Ctrl Pts',(179.685275566044,-5.91010297967495,334.678851230667));
#8610=CARTESIAN_POINT('Ctrl Pts',(179.677865662194,-5.91445973306567,334.835389464357));
#8611=CARTESIAN_POINT('Ctrl Pts',(179.675261109697,-5.91599111500422,334.890412047061));
#8612=CARTESIAN_POINT('Ctrl Pts',(179.6726565572,-5.91675383644239,334.945428057878));
#8613=CARTESIAN_POINT('Ctrl Pts',(179.670052004703,-5.91674998548957,335.000414378067));
#8614=CARTESIAN_POINT('',(177.920052775238,-5.91497190102853,334.994674821255));
#8615=CARTESIAN_POINT('Ctrl Pts',(179.670052004703,-5.92646392270013,335.00041505838));
#8616=CARTESIAN_POINT('Ctrl Pts',(179.669006712142,-5.92648621669284,335.022519108687));
#8617=CARTESIAN_POINT('Ctrl Pts',(179.667961419581,-5.92637327756805,335.044622924713));
#8618=CARTESIAN_POINT('Ctrl Pts',(179.574170115596,-5.90404367840924,337.027801861348));
#8619=CARTESIAN_POINT('Ctrl Pts',(179.388678092746,-3.71978762975183,340.92585884392));
#8620=CARTESIAN_POINT('Ctrl Pts',(179.110440058472,2.97019053767725,341.334871015977));
#8621=CARTESIAN_POINT('Ctrl Pts',(178.832202024198,6.93446874656139,335.930465615495));
#8622=CARTESIAN_POINT('Ctrl Pts',(178.553963989924,4.53508730863143,329.672185623518));
#8623=CARTESIAN_POINT('Ctrl Pts',(178.27572595565,-2.02607679839931,328.303162262213));
#8624=CARTESIAN_POINT('Ctrl Pts',(178.064422347311,-5.59683481069391,331.930651892861));
#8625=CARTESIAN_POINT('Ctrl Pts',(177.945864750396,-5.91882038961358,334.445878104145));
#8626=CARTESIAN_POINT('Ctrl Pts',(177.920053164906,-5.91407390179608,334.994667342421));
#8627=CARTESIAN_POINT('',(176.170051188577,-5.91178907071594,335.002177354139));
#8628=CARTESIAN_POINT('Ctrl Pts',(177.920052004703,-5.91674761691405,334.994689610001));
#8629=CARTESIAN_POINT('Ctrl Pts',(177.912714213781,-5.91688770210566,335.150770184837));
#8630=CARTESIAN_POINT('Ctrl Pts',(177.905376422858,-5.91084758222949,335.306982769653));
#8631=CARTESIAN_POINT('Ctrl Pts',(177.898038631936,-5.89862280926592,335.462795328961));
#8632=CARTESIAN_POINT('Ctrl Pts',(177.890589100901,-5.88621187707302,335.620980606849));
#8633=CARTESIAN_POINT('Ctrl Pts',(177.883139569866,-5.86742635957227,335.778753179454));
#8634=CARTESIAN_POINT('Ctrl Pts',(177.875690038832,-5.84231658479985,335.935557312767));
#8635=CARTESIAN_POINT('Ctrl Pts',(177.868356772245,-5.81759869699262,336.089914212026));
#8636=CARTESIAN_POINT('Ctrl Pts',(177.861023505659,-5.7867525997992,336.243332296058));
#8637=CARTESIAN_POINT('Ctrl Pts',(177.853690239072,-5.74987839465665,336.395288145567));
#8638=CARTESIAN_POINT('Ctrl Pts',(177.846356943828,-5.71300404541406,336.547244588902));
#8639=CARTESIAN_POINT('Ctrl Pts',(177.839023648584,-5.67010163064186,336.697738416624));
#8640=CARTESIAN_POINT('Ctrl Pts',(177.83169035334,-5.62132192356637,336.846258485189));
#8641=CARTESIAN_POINT('Ctrl Pts',(177.824355520482,-5.57253198857071,336.994809694806));
#8642=CARTESIAN_POINT('Ctrl Pts',(177.817020687624,-5.51786242740262,337.141385960352));
#8643=CARTESIAN_POINT('Ctrl Pts',(177.809685854766,-5.45751314636585,337.285493561519));
#8644=CARTESIAN_POINT('Ctrl Pts',(177.802149524128,-5.39550598894267,337.433559993428));
#8645=CARTESIAN_POINT('Ctrl Pts',(177.794613193489,-5.32750272876749,337.579019778803));
#8646=CARTESIAN_POINT('Ctrl Pts',(177.787076862851,-5.25377157600491,337.721362671469));
#8647=CARTESIAN_POINT('Ctrl Pts',(177.779730623447,-5.1819001672736,337.860115204631));
#8648=CARTESIAN_POINT('Ctrl Pts',(177.772384384044,-5.10458658987453,337.995905893275));
#8649=CARTESIAN_POINT('Ctrl Pts',(177.765038144641,-5.02212389008489,338.128290618715));
#8650=CARTESIAN_POINT('Ctrl Pts',(177.757406768385,-4.93646048399682,338.265813723393));
#8651=CARTESIAN_POINT('Ctrl Pts',(177.749775392128,-4.84524047988318,338.399660775208));
#8652=CARTESIAN_POINT('Ctrl Pts',(177.742144015872,-4.74883867014821,338.529371310503));
#8653=CARTESIAN_POINT('Ctrl Pts',(177.734512639616,-4.65243686041325,338.659081845799));
#8654=CARTESIAN_POINT('Ctrl Pts',(177.726881263359,-4.55085358558808,338.784655558879));
#8655=CARTESIAN_POINT('Ctrl Pts',(177.719249887103,-4.44450602610207,338.905674941216));
#8656=CARTESIAN_POINT('Ctrl Pts',(177.711825909658,-4.34104868676153,339.023405365551));
#8657=CARTESIAN_POINT('Ctrl Pts',(177.704401932212,-4.23275420849354,339.137199834385));
#8658=CARTESIAN_POINT('Ctrl Pts',(177.696977954767,-4.11995369376139,339.246635388606));
#8659=CARTESIAN_POINT('Ctrl Pts',(177.689562738732,-4.00728630060703,339.35594179241));
#8660=CARTESIAN_POINT('Ctrl Pts',(177.682147522697,-3.89012372141636,339.460899263816));
#8661=CARTESIAN_POINT('Ctrl Pts',(177.674732306662,-3.76883708465367,339.561118019942));
#8662=CARTESIAN_POINT('Ctrl Pts',(177.66732422551,-3.64766714928069,339.661240346087));
#8663=CARTESIAN_POINT('Ctrl Pts',(177.659916144359,-3.52238134195654,339.756632798064));
#8664=CARTESIAN_POINT('Ctrl Pts',(177.652508063207,-3.39338730933572,339.846942658144));
#8665=CARTESIAN_POINT('Ctrl Pts',(177.645105496026,-3.26448928932791,339.937185298948));
#8666=CARTESIAN_POINT('Ctrl Pts',(177.637702928844,-3.13188884420546,340.022352667362));
#8667=CARTESIAN_POINT('Ctrl Pts',(177.630300361662,-2.99602625007755,340.102132619929));
#8668=CARTESIAN_POINT('Ctrl Pts',(177.6229016919,-2.86023518700992,340.181870568701));
#8669=CARTESIAN_POINT('Ctrl Pts',(177.615503022138,-2.72118571647128,340.256226562082));
#8670=CARTESIAN_POINT('Ctrl Pts',(177.608104352375,-2.57934651572282,340.324932122979));
#8671=CARTESIAN_POINT('Ctrl Pts',(177.600706903163,-2.43753071403716,340.393626349591));
#8672=CARTESIAN_POINT('Ctrl Pts',(177.593309453952,-2.29292643108194,340.456671831188));
#8673=CARTESIAN_POINT('Ctrl Pts',(177.58591200474,-2.14602643635296,340.513846306978));
#8674=CARTESIAN_POINT('Ctrl Pts',(177.578514876269,-1.99913281095101,340.571018303783));
#8675=CARTESIAN_POINT('Ctrl Pts',(177.571117747798,-1.84994401948705,340.622319665558));
#8676=CARTESIAN_POINT('Ctrl Pts',(177.563720619326,-1.69897202381249,340.667576609522));
#8677=CARTESIAN_POINT('Ctrl Pts',(177.556322351882,-1.54797678221842,340.712840521926));
#8678=CARTESIAN_POINT('Ctrl Pts',(177.548924084438,-1.39519814722675,340.752058056221));
#8679=CARTESIAN_POINT('Ctrl Pts',(177.541525816993,-1.24116227569561,340.785105596952));
#8680=CARTESIAN_POINT('Ctrl Pts',(177.53412495046,-1.08707228974226,340.818164747632));
#8681=CARTESIAN_POINT('Ctrl Pts',(177.526724083926,-0.931724552542117,340.845049510853));
#8682=CARTESIAN_POINT('Ctrl Pts',(177.519323217392,-0.775654270532592,340.865687599515));
#8683=CARTESIAN_POINT('Ctrl Pts',(177.511914224,-0.619412608432403,340.886348350772));
#8684=CARTESIAN_POINT('Ctrl Pts',(177.504505230607,-0.462447187225275,340.900748679835));
#8685=CARTESIAN_POINT('Ctrl Pts',(177.497096237215,-0.305297914327727,340.908868228858));
#8686=CARTESIAN_POINT('Ctrl Pts',(177.489682679627,-0.148051832057079,340.916992779803));
#8687=CARTESIAN_POINT('Ctrl Pts',(177.482269122039,0.00937795527349783,
340.918828836519));
#8688=CARTESIAN_POINT('Ctrl Pts',(177.47485556445,0.166453214854142,340.914408160566));
#8689=CARTESIAN_POINT('Ctrl Pts',(177.467431452306,0.323752099822014,340.909981190971));
#8690=CARTESIAN_POINT('Ctrl Pts',(177.460007340161,0.48069507764046,340.899279723761));
#8691=CARTESIAN_POINT('Ctrl Pts',(177.452583228017,0.636749875160684,340.882387284002));
#8692=CARTESIAN_POINT('Ctrl Pts',(177.448726102954,0.717826623318829,340.873610981664));
#8693=CARTESIAN_POINT('Ctrl Pts',(177.444868977892,0.798663802018155,340.863164441332));
#8694=CARTESIAN_POINT('Ctrl Pts',(177.441011852829,0.879188145233416,340.851064755049));
#8695=CARTESIAN_POINT('Ctrl Pts',(177.433587875393,1.03417687320687,340.827775959252));
#8696=CARTESIAN_POINT('Ctrl Pts',(177.426163897958,1.18847342566624,340.798289538784));
#8697=CARTESIAN_POINT('Ctrl Pts',(177.418739920522,1.34154294873124,340.762655037325));
#8698=CARTESIAN_POINT('Ctrl Pts',(177.411324704496,1.49443182672829,340.72706258994));
#8699=CARTESIAN_POINT('Ctrl Pts',(177.403909488471,1.64609619779929,340.685336587869));
#8700=CARTESIAN_POINT('Ctrl Pts',(177.396494272445,1.79600744629644,340.637578187072));
#8701=CARTESIAN_POINT('Ctrl Pts',(177.389086191303,1.94577445094465,340.589865739167));
#8702=CARTESIAN_POINT('Ctrl Pts',(177.381678110161,2.09379133798909,340.536132560432));
#8703=CARTESIAN_POINT('Ctrl Pts',(177.374270029019,2.23954089857283,340.476530573832));
#8704=CARTESIAN_POINT('Ctrl Pts',(177.366867461847,2.38518197509642,340.41697295008));
#8705=CARTESIAN_POINT('Ctrl Pts',(177.359464894675,2.52855874147771,340.351555356964));
#8706=CARTESIAN_POINT('Ctrl Pts',(177.352062327504,2.66917045095894,340.280479113322));
#8707=CARTESIAN_POINT('Ctrl Pts',(177.344663657751,2.80970812898883,340.209440291012));
#8708=CARTESIAN_POINT('Ctrl Pts',(177.337264987998,2.94748331717329,340.132748919477));
#8709=CARTESIAN_POINT('Ctrl Pts',(177.329866318246,3.08201661923865,340.050653831064));
#8710=CARTESIAN_POINT('Ctrl Pts',(177.322468869044,3.21652772748755,339.96857228579));
#8711=CARTESIAN_POINT('Ctrl Pts',(177.315071419842,3.34779769277276,339.881088987085));
#8712=CARTESIAN_POINT('Ctrl Pts',(177.30767397064,3.47537294540474,339.788498037261));
#8713=CARTESIAN_POINT('Ctrl Pts',(177.300276842179,3.60294266659611,339.695911102019));
#8714=CARTESIAN_POINT('Ctrl Pts',(177.292879713718,3.72681769161282,339.598217175208));
#8715=CARTESIAN_POINT('Ctrl Pts',(177.285482585256,3.84657483087278,339.495752732635));
#8716=CARTESIAN_POINT('Ctrl Pts',(177.278084317822,3.96635040974271,339.393272513096));
#8717=CARTESIAN_POINT('Ctrl Pts',(177.270686050387,4.08200655677947,339.286020557874));
#8718=CARTESIAN_POINT('Ctrl Pts',(177.263287782953,4.19315458744328,339.174372428079));
#8719=CARTESIAN_POINT('Ctrl Pts',(177.255886916429,4.30434166557978,339.062685075121));
#8720=CARTESIAN_POINT('Ctrl Pts',(177.248486049906,4.411017210961,338.946598736973));
#8721=CARTESIAN_POINT('Ctrl Pts',(177.241085183382,4.51283080491,338.826524361448));
#8722=CARTESIAN_POINT('Ctrl Pts',(177.233676189999,4.61475619991864,338.70631813278));
#8723=CARTESIAN_POINT('Ctrl Pts',(177.226267196617,4.71180873994169,338.582115405971));
#8724=CARTESIAN_POINT('Ctrl Pts',(177.218858203234,4.8036791307486,338.454359183888));
#8725=CARTESIAN_POINT('Ctrl Pts',(177.211444645656,4.89560611688486,338.326524259565));
#8726=CARTESIAN_POINT('Ctrl Pts',(177.204031088078,4.98234438742863,338.195131788682));
#8727=CARTESIAN_POINT('Ctrl Pts',(177.1966175305,5.06362938269769,338.060651570692));
#8728=CARTESIAN_POINT('Ctrl Pts',(177.189193418365,5.14503010203933,337.925979895491));
#8729=CARTESIAN_POINT('Ctrl Pts',(177.18176930623,5.22096186071101,337.788212019519));
#8730=CARTESIAN_POINT('Ctrl Pts',(177.174345194096,5.29120685317979,337.647840742825));
#8731=CARTESIAN_POINT('Ctrl Pts',(177.170488068916,5.3277019551287,337.574912212639));
#8732=CARTESIAN_POINT('Ctrl Pts',(177.166630943735,5.36266287344064,337.501281279861));
#8733=CARTESIAN_POINT('Ctrl Pts',(177.162773818555,5.39606433272757,337.427018804947));
#8734=CARTESIAN_POINT('Ctrl Pts',(177.155349841118,5.46035358146345,337.284082573314));
#8735=CARTESIAN_POINT('Ctrl Pts',(177.147925863681,5.51905653950395,337.138374516508));
#8736=CARTESIAN_POINT('Ctrl Pts',(177.140501886244,5.57192542906149,336.990371215497));
#8737=CARTESIAN_POINT('Ctrl Pts',(177.133086670217,5.62473192537479,336.842542580649));
#8738=CARTESIAN_POINT('Ctrl Pts',(177.12567145419,5.67171793373778,336.692424441415));
#8739=CARTESIAN_POINT('Ctrl Pts',(177.118256238164,5.71268245409505,336.540516063264));
#8740=CARTESIAN_POINT('Ctrl Pts',(177.11084815702,5.75360755859698,336.38875385059));
#8741=CARTESIAN_POINT('Ctrl Pts',(177.103440075877,5.78852261303763,336.235205186225));
#8742=CARTESIAN_POINT('Ctrl Pts',(177.096031994734,5.81727548129005,336.080387216363));
#8743=CARTESIAN_POINT('Ctrl Pts',(177.088629427561,5.84600694825745,335.925684480345));
#8744=CARTESIAN_POINT('Ctrl Pts',(177.081226860388,5.86858529382467,335.769714685365));
#8745=CARTESIAN_POINT('Ctrl Pts',(177.073824293215,5.88490882849242,335.613007865228));
#8746=CARTESIAN_POINT('Ctrl Pts',(177.066425623461,5.90122376889044,335.456383550549));
#8747=CARTESIAN_POINT('Ctrl Pts',(177.059026953707,5.91129041828467,335.299023353787));
#8748=CARTESIAN_POINT('Ctrl Pts',(177.051628283953,5.91505859627196,335.141465066957));
#8749=CARTESIAN_POINT('Ctrl Pts',(177.04423083475,5.9188261526269,334.983932772352));
#8750=CARTESIAN_POINT('Ctrl Pts',(177.036833385547,5.9162972908433,334.826202825278));
#8751=CARTESIAN_POINT('Ctrl Pts',(177.029435936344,5.90747387524594,334.6688157978));
#8752=CARTESIAN_POINT('Ctrl Pts',(177.022038807882,5.89865084221655,334.51143559435));
#8753=CARTESIAN_POINT('Ctrl Pts',(177.014641679419,5.8835338189202,334.35439865356));
#8754=CARTESIAN_POINT('Ctrl Pts',(177.007244550957,5.86217674287609,334.198242930943));
#8755=CARTESIAN_POINT('Ctrl Pts',(176.999846283521,5.84081637837532,334.042063164243));
#8756=CARTESIAN_POINT('Ctrl Pts',(176.992448016085,5.81321409859842,333.886765255675));
#8757=CARTESIAN_POINT('Ctrl Pts',(176.98504974865,5.77947538138788,333.732879296029));
#8758=CARTESIAN_POINT('Ctrl Pts',(176.977648882125,5.74572481141134,333.578939274628));
#8759=CARTESIAN_POINT('Ctrl Pts',(176.9702480156,5.70583359169296,333.426412554071));
#8760=CARTESIAN_POINT('Ctrl Pts',(176.962847149075,5.65995766536272,333.27581619634));
#8761=CARTESIAN_POINT('Ctrl Pts',(176.955438155691,5.61403136287951,333.125054469412));
#8762=CARTESIAN_POINT('Ctrl Pts',(176.948029162308,5.56210733841011,332.976227695737));
#8763=CARTESIAN_POINT('Ctrl Pts',(176.940620168924,5.50439074565899,332.829835701703));
#8764=CARTESIAN_POINT('Ctrl Pts',(176.933206611345,5.44663859749561,332.68335352515));
#8765=CARTESIAN_POINT('Ctrl Pts',(176.925793053765,5.38308692079485,332.53930945766));
#8766=CARTESIAN_POINT('Ctrl Pts',(176.918379496186,5.31398761151646,332.398180208556));
#8767=CARTESIAN_POINT('Ctrl Pts',(176.91095538405,5.24478992672144,332.25685003613));
#8768=CARTESIAN_POINT('Ctrl Pts',(176.903531271915,5.17002901221364,332.11844329751));
#8769=CARTESIAN_POINT('Ctrl Pts',(176.896107159779,5.09000140699761,331.9834098324));
#8770=CARTESIAN_POINT('Ctrl Pts',(176.892250034613,5.04842384399744,331.913254510526));
#8771=CARTESIAN_POINT('Ctrl Pts',(176.888392909447,5.0054253808852,331.844009206049));
#8772=CARTESIAN_POINT('Ctrl Pts',(176.884535784281,4.96105192776692,331.775733520241));
#8773=CARTESIAN_POINT('Ctrl Pts',(176.877111806842,4.87564440255624,331.644320322773));
#8774=CARTESIAN_POINT('Ctrl Pts',(176.869687829403,4.78488292798476,331.516104762685));
#8775=CARTESIAN_POINT('Ctrl Pts',(176.862263851964,4.68903418437665,331.391553106911));
#8776=CARTESIAN_POINT('Ctrl Pts',(176.854848635935,4.59329855670691,331.267148440829));
#8777=CARTESIAN_POINT('Ctrl Pts',(176.847433419907,4.49248783594312,331.146399365049));
#8778=CARTESIAN_POINT('Ctrl Pts',(176.840018203878,4.38691309240689,331.029745085996));
#8779=CARTESIAN_POINT('Ctrl Pts',(176.832610122733,4.28143993235722,330.913203051104));
#8780=CARTESIAN_POINT('Ctrl Pts',(176.825202041588,4.17121212402109,330.800748244013));
#8781=CARTESIAN_POINT('Ctrl Pts',(176.817793960442,4.0565822170802,330.692788456719));
#8782=CARTESIAN_POINT('Ctrl Pts',(176.810391393267,3.94203763127248,330.584909025867));
#8783=CARTESIAN_POINT('Ctrl Pts',(176.802988826092,3.82309774149546,330.481518207766));
#8784=CARTESIAN_POINT('Ctrl Pts',(176.795586258917,3.7001532344614,330.382988346993));
#8785=CARTESIAN_POINT('Ctrl Pts',(176.788187589161,3.57727345717211,330.284510361759));
#8786=CARTESIAN_POINT('Ctrl Pts',(176.780788919405,3.45039355215038,330.190888469716));
#8787=CARTESIAN_POINT('Ctrl Pts',(176.773390249649,3.31993860467935,330.102455898753));
#8788=CARTESIAN_POINT('Ctrl Pts',(176.765992800444,3.18950517822406,330.014037916418));
#8789=CARTESIAN_POINT('Ctrl Pts',(176.758595351239,3.05549818844676,329.930807765335));
#8790=CARTESIAN_POINT('Ctrl Pts',(176.751197902034,2.91837322282364,329.853056412316));
#8791=CARTESIAN_POINT('Ctrl Pts',(176.743800773569,2.78125420269984,329.77530843046));
#8792=CARTESIAN_POINT('Ctrl Pts',(176.736403645105,2.64101780018663,329.70303895842));
#8793=CARTESIAN_POINT('Ctrl Pts',(176.72900651664,2.49814558223962,329.636493757584));
#8794=CARTESIAN_POINT('Ctrl Pts',(176.721608249202,2.35525136553741,329.569938310448));
#8795=CARTESIAN_POINT('Ctrl Pts',(176.714209981765,2.20972086363594,329.509109047073));
#8796=CARTESIAN_POINT('Ctrl Pts',(176.706811714327,2.06205692130117,329.454204131433));
#8797=CARTESIAN_POINT('Ctrl Pts',(176.6994108478,1.91434110307088,329.399279927119));
#8798=CARTESIAN_POINT('Ctrl Pts',(176.692009981273,1.76449070174616,329.350284344364));
#8799=CARTESIAN_POINT('Ctrl Pts',(176.684609114746,1.61302491555565,329.307366059169));
#8800=CARTESIAN_POINT('Ctrl Pts',(176.67720012136,1.46139280545063,329.264400645595));
#8801=CARTESIAN_POINT('Ctrl Pts',(176.669791127974,1.30814212730147,329.22752595863));
#8802=CARTESIAN_POINT('Ctrl Pts',(176.662382134588,1.15380421622146,329.196839964887));
#8803=CARTESIAN_POINT('Ctrl Pts',(176.654968577007,0.999371227664755,329.166135067514));
#8804=CARTESIAN_POINT('Ctrl Pts',(176.647555019426,0.843850039366241,329.141626518131));
#8805=CARTESIAN_POINT('Ctrl Pts',(176.640141461844,0.687777841723747,329.12336046682));
#8806=CARTESIAN_POINT('Ctrl Pts',(176.632717349706,0.531483446735364,329.105068410441));
#8807=CARTESIAN_POINT('Ctrl Pts',(176.625293237569,0.3746368467885,329.093036630397));
#8808=CARTESIAN_POINT('Ctrl Pts',(176.617869125431,0.217776795958029,329.087259194786));
#8809=CARTESIAN_POINT('Ctrl Pts',(176.61401200029,0.136281684561534,329.084257584394));
#8810=CARTESIAN_POINT('Ctrl Pts',(176.610154875148,0.0547828956273552,329.082943301829));
#8811=CARTESIAN_POINT('Ctrl Pts',(176.606297750007,-0.0266446062728537,
329.08330999397));
#8812=CARTESIAN_POINT('Ctrl Pts',(176.59887377257,-0.183371680141186,329.08401578237));
#8813=CARTESIAN_POINT('Ctrl Pts',(176.591449795132,-0.3403071217284,329.090954246073));
#8814=CARTESIAN_POINT('Ctrl Pts',(176.584025817694,-0.496914521196266,329.104153451698));
#8815=CARTESIAN_POINT('Ctrl Pts',(176.576610601667,-0.65333710036991,329.117337080274));
#8816=CARTESIAN_POINT('Ctrl Pts',(176.56919538564,-0.80943203975444,329.136766712572));
#8817=CARTESIAN_POINT('Ctrl Pts',(176.561780169613,-0.96466166329435,329.162418442722));
#8818=CARTESIAN_POINT('Ctrl Pts',(176.554372088469,-1.1197419256715,329.188045490907));
#8819=CARTESIAN_POINT('Ctrl Pts',(176.546964007325,-1.27395816400389,329.219882657757));
#8820=CARTESIAN_POINT('Ctrl Pts',(176.539555926182,-1.4267766724408,329.257854156373));
#8821=CARTESIAN_POINT('Ctrl Pts',(176.532153359008,-1.57948143527166,329.29579739211));
#8822=CARTESIAN_POINT('Ctrl Pts',(176.524750791834,-1.73079017906078,329.339865778638));
#8823=CARTESIAN_POINT('Ctrl Pts',(176.517348224661,-1.88017836831403,329.389932276182));
#8824=CARTESIAN_POINT('Ctrl Pts',(176.509949554906,-2.02948790533859,329.439972413934));
#8825=CARTESIAN_POINT('Ctrl Pts',(176.502550885152,-2.17687854864409,329.496004255101));
#8826=CARTESIAN_POINT('Ctrl Pts',(176.495152215398,-2.32184004175152,329.557850665131));
#8827=CARTESIAN_POINT('Ctrl Pts',(176.487754766194,-2.46677762071338,329.619686872423));
#8828=CARTESIAN_POINT('Ctrl Pts',(176.48035731699,-2.60928650186431,329.687335598518));
#8829=CARTESIAN_POINT('Ctrl Pts',(176.472959867787,-2.74887546047948,329.760571189025));
#8830=CARTESIAN_POINT('Ctrl Pts',(176.465562739324,-2.88845836676082,329.833803604165));
#8831=CARTESIAN_POINT('Ctrl Pts',(176.458165610861,-3.02512127174652,329.912622228679));
#8832=CARTESIAN_POINT('Ctrl Pts',(176.450768482397,-3.15839690593207,329.996755098229));
#8833=CARTESIAN_POINT('Ctrl Pts',(176.443370214961,-3.29169306123805,330.080900922141));
#8834=CARTESIAN_POINT('Ctrl Pts',(176.435971947525,-3.42160059164968,330.170362421119));
#8835=CARTESIAN_POINT('Ctrl Pts',(176.428573680089,-3.54768073869756,330.26482398017));
#8836=CARTESIAN_POINT('Ctrl Pts',(176.421172813563,-3.67380517902699,330.35931872456));
#8837=CARTESIAN_POINT('Ctrl Pts',(176.413771947038,-3.79609926040344,330.458816802721));
#8838=CARTESIAN_POINT('Ctrl Pts',(176.406371080513,-3.91415699005094,330.562962066904));
#8839=CARTESIAN_POINT('Ctrl Pts',(176.398962087128,-4.03234435837296,330.667221692543));
#8840=CARTESIAN_POINT('Ctrl Pts',(176.391553093744,-4.14628580479258,330.776138448235));
#8841=CARTESIAN_POINT('Ctrl Pts',(176.38414410036,-4.25561141117888,330.889318538302));
#8842=CARTESIAN_POINT('Ctrl Pts',(176.37673054278,-4.36500436590949,331.002568351209));
#8843=CARTESIAN_POINT('Ctrl Pts',(176.3693169852,-4.46977556674499,331.120086453936));
#8844=CARTESIAN_POINT('Ctrl Pts',(176.36190342762,-4.56959550054893,331.241446086077));
#8845=CARTESIAN_POINT('Ctrl Pts',(176.354479315484,-4.66955754630326,331.362978495873));
#8846=CARTESIAN_POINT('Ctrl Pts',(176.347055203347,-4.76455402192201,331.488363061336));
#8847=CARTESIAN_POINT('Ctrl Pts',(176.339631091211,-4.85429836492277,331.617143522582));
#8848=CARTESIAN_POINT('Ctrl Pts',(176.335773966052,-4.90092416433609,331.684050157069));
#8849=CARTESIAN_POINT('Ctrl Pts',(176.331916840892,-4.94613304389588,331.75187299399));
#8850=CARTESIAN_POINT('Ctrl Pts',(176.328059715733,-4.98988977844441,331.820545555999));
#8851=CARTESIAN_POINT('Ctrl Pts',(176.320453925922,-5.07617282917936,331.955959640553));
#8852=CARTESIAN_POINT('Ctrl Pts',(176.31284813611,-5.15705683796547,332.095071661292));
#8853=CARTESIAN_POINT('Ctrl Pts',(176.305242346299,-5.23221784202617,332.237423844293));
#8854=CARTESIAN_POINT('Ctrl Pts',(176.297646843112,-5.30727719286556,332.379583499823));
#8855=CARTESIAN_POINT('Ctrl Pts',(176.290051339925,-5.3766287945708,332.524974283587));
#8856=CARTESIAN_POINT('Ctrl Pts',(176.282455836739,-5.43999184926805,332.673109533649));
#8857=CARTESIAN_POINT('Ctrl Pts',(176.274869399746,-5.50327927214354,332.821067965548));
#8858=CARTESIAN_POINT('Ctrl Pts',(176.267282962753,-5.560592251189,332.971764019555));
#8859=CARTESIAN_POINT('Ctrl Pts',(176.25969652576,-5.61169576389038,333.124686368621));
#8860=CARTESIAN_POINT('Ctrl Pts',(176.252120196404,-5.66273118985307,333.277404974667));
#8861=CARTESIAN_POINT('Ctrl Pts',(176.244543867048,-5.70757353449418,333.432343632674));
#8862=CARTESIAN_POINT('Ctrl Pts',(176.236967537693,-5.74603589713926,333.588971286158));
#8863=CARTESIAN_POINT('Ctrl Pts',(176.22939711922,-5.78446825230645,333.745476742238));
#8864=CARTESIAN_POINT('Ctrl Pts',(176.221826700747,-5.81653045695088,333.903668231897));
#8865=CARTESIAN_POINT('Ctrl Pts',(176.214256282275,-5.8420852177126,334.062999001343));
#8866=CARTESIAN_POINT('Ctrl Pts',(176.206691491682,-5.86762098096063,334.222211323644));
#8867=CARTESIAN_POINT('Ctrl Pts',(176.19912670109,-5.88665888814513,334.382560894078));
#8868=CARTESIAN_POINT('Ctrl Pts',(176.191561910497,-5.89911259517965,334.543490249948));
#8869=CARTESIAN_POINT('Ctrl Pts',(176.184391941899,-5.91091631760589,334.696020371433));
#8870=CARTESIAN_POINT('Ctrl Pts',(176.177221973301,-5.91680553894543,334.849070998502));
#8871=CARTESIAN_POINT('Ctrl Pts',(176.170052004703,-5.91674960508396,335.002161767525));
#8872=CARTESIAN_POINT('',(174.420052004703,-5.922005427706,335.004419719925));
#8873=CARTESIAN_POINT('Ctrl Pts',(176.170050516938,-5.90770675093187,335.002190181294));
#8874=CARTESIAN_POINT('Ctrl Pts',(176.129974238446,-5.91049512676808,335.856578754585));
#8875=CARTESIAN_POINT('Ctrl Pts',(175.997151948527,-5.33684541281739,338.684647950317));
#8876=CARTESIAN_POINT('Ctrl Pts',(175.771583647186,-0.977291647241818,341.928024534987));
#8877=CARTESIAN_POINT('Ctrl Pts',(175.493345612911,5.29705504710014,339.570977001614));
#8878=CARTESIAN_POINT('Ctrl Pts',(175.215107578637,6.71037250910805,333.019211341358));
#8879=CARTESIAN_POINT('Ctrl Pts',(174.936869544363,1.96568016445112,328.285186196753));
#8880=CARTESIAN_POINT('Ctrl Pts',(174.671851019719,-4.27175548752083,329.64539726177));
#8881=CARTESIAN_POINT('Ctrl Pts',(174.499578506499,-5.90796248829746,333.31938805982));
#8882=CARTESIAN_POINT('Ctrl Pts',(174.420052004703,-5.922005427706,335.004419719925));
#8883=CARTESIAN_POINT('',(172.670052004703,-5.92176215774818,334.995489375811));
#8884=CARTESIAN_POINT('Ctrl Pts',(174.420052004703,-5.922005427706,335.004419719925));
#8885=CARTESIAN_POINT('Ctrl Pts',(174.406832495074,-5.9243397536042,335.284518702699));
#8886=CARTESIAN_POINT('Ctrl Pts',(174.300866974022,-5.77886390257711,337.527311927912));
#8887=CARTESIAN_POINT('Ctrl Pts',(174.102155441539,-2.91301564628694,341.361364850856));
#8888=CARTESIAN_POINT('Ctrl Pts',(173.823917407268,3.77300750184398,340.892116539262));
#8889=CARTESIAN_POINT('Ctrl Pts',(173.545679372993,6.99659735503171,335.015759847085));
#8890=CARTESIAN_POINT('Ctrl Pts',(173.26744133872,3.79951308511499,329.124940575853));
#8891=CARTESIAN_POINT('Ctrl Pts',(172.989203304447,-2.88432826229091,328.625576622425));
#8892=CARTESIAN_POINT('Ctrl Pts',(172.790073526441,-5.77348806552616,332.454722659356));
#8893=CARTESIAN_POINT('Ctrl Pts',(172.68368975986,-5.92420449000434,334.706497575313));
#8894=CARTESIAN_POINT('Ctrl Pts',(172.670052004703,-5.92176215774818,334.995489375811));
#8895=CARTESIAN_POINT('',(170.920052775829,-5.91174205618225,334.997960046411));
#8896=CARTESIAN_POINT('Ctrl Pts',(172.670052004703,-5.92176215774818,334.995489375811));
#8897=CARTESIAN_POINT('Ctrl Pts',(172.590943748435,-5.90759496939487,336.671838390109));
#8898=CARTESIAN_POINT('Ctrl Pts',(172.419089480741,-4.28600052805519,340.337495202448));
#8899=CARTESIAN_POINT('Ctrl Pts',(172.154489201625,1.93541011290003,341.723601015535));
#8900=CARTESIAN_POINT('Ctrl Pts',(171.87625116735,6.70138100159934,337.01099865555));
#8901=CARTESIAN_POINT('Ctrl Pts',(171.598013133077,5.31759345735263,330.452932511658));
#8902=CARTESIAN_POINT('Ctrl Pts',(171.319775098802,-0.946071115155991,328.067643087211));
#8903=CARTESIAN_POINT('Ctrl Pts',(171.093788525015,-5.32830294487111,331.297324785966));
#8904=CARTESIAN_POINT('Ctrl Pts',(170.960547962653,-5.91024973360072,334.134607831533));
#8905=CARTESIAN_POINT('Ctrl Pts',(170.920053411716,-5.90761268027711,334.997947902807));
#8906=CARTESIAN_POINT('',(169.170051282952,-5.91509985026952,335.005356513866));
#8907=CARTESIAN_POINT('Ctrl Pts',(170.920052004704,-5.91674965339537,334.997974772674));
#8908=CARTESIAN_POINT('Ctrl Pts',(170.912477675923,-5.91680501271475,335.159708336888));
#8909=CARTESIAN_POINT('Ctrl Pts',(170.904903347141,-5.91022456887072,335.321391389275));
#8910=CARTESIAN_POINT('Ctrl Pts',(170.89732901836,-5.89704707365479,335.482458675535));
#8911=CARTESIAN_POINT('Ctrl Pts',(170.889750598561,-5.88386246106037,335.643612956844));
#8912=CARTESIAN_POINT('Ctrl Pts',(170.882172178762,-5.86407372135668,335.804150462569));
#8913=CARTESIAN_POINT('Ctrl Pts',(170.874593758963,-5.83777137120097,335.963512314445));
#8914=CARTESIAN_POINT('Ctrl Pts',(170.867010072625,-5.81145074251618,336.122984913087));
#8915=CARTESIAN_POINT('Ctrl Pts',(170.859426386286,-5.77860753502681,336.281279886438));
#8916=CARTESIAN_POINT('Ctrl Pts',(170.851842699948,-5.73938316122999,336.437849606562));
#8917=CARTESIAN_POINT('Ctrl Pts',(170.84424690036,-5.70009613523716,336.594669411922));
#8918=CARTESIAN_POINT('Ctrl Pts',(170.836651100773,-5.65440765824046,336.749758119261));
#8919=CARTESIAN_POINT('Ctrl Pts',(170.829055301185,-5.60250914744104,336.902582932579));
#8920=CARTESIAN_POINT('Ctrl Pts',(170.821453175153,-5.55056741103452,337.055535031732));
#8921=CARTESIAN_POINT('Ctrl Pts',(170.813851049122,-5.49240544938,337.206219152313));
#8922=CARTESIAN_POINT('Ctrl Pts',(170.80624892309,-5.42826245886085,337.354123454754));
#8923=CARTESIAN_POINT('Ctrl Pts',(170.79863257236,-5.36399944735397,337.50230450794));
#8924=CARTESIAN_POINT('Ctrl Pts',(170.79101622163,-5.29373318599943,337.647695031932));
#8925=CARTESIAN_POINT('Ctrl Pts',(170.7833998709,-5.21774912932506,337.789807266807));
#8926=CARTESIAN_POINT('Ctrl Pts',(170.776699590685,-5.15090419404948,337.914826692695));
#8927=CARTESIAN_POINT('Ctrl Pts',(170.76999931047,-5.07963493900917,338.037309289029));
#8928=CARTESIAN_POINT('Ctrl Pts',(170.763299030255,-5.00416252374732,338.1569428247));
#8929=CARTESIAN_POINT('Ctrl Pts',(170.755875052817,-4.92053833339655,338.289497977792));
#8930=CARTESIAN_POINT('Ctrl Pts',(170.748451075379,-4.83151747874265,338.418928123214));
#8931=CARTESIAN_POINT('Ctrl Pts',(170.741027097941,-4.73736031598068,338.544763433443));
#8932=CARTESIAN_POINT('Ctrl Pts',(170.733611881913,-4.64331427283756,338.670450239072));
#8933=CARTESIAN_POINT('Ctrl Pts',(170.726196665886,-4.54414420874919,338.792550358252));
#8934=CARTESIAN_POINT('Ctrl Pts',(170.718781449858,-4.44015523147386,338.910620421738));
#8935=CARTESIAN_POINT('Ctrl Pts',(170.711373368714,-4.33626631186883,339.028576878804));
#8936=CARTESIAN_POINT('Ctrl Pts',(170.70396528757,-4.22756795497178,339.142510721752));
#8937=CARTESIAN_POINT('Ctrl Pts',(170.696557206426,-4.11440716855892,339.25200943247));
#8938=CARTESIAN_POINT('Ctrl Pts',(170.689154639252,-4.00133060978618,339.361426641297));
#8939=CARTESIAN_POINT('Ctrl Pts',(170.681752072078,-3.88379850207925,339.466415032553));
#8940=CARTESIAN_POINT('Ctrl Pts',(170.674349504904,-3.76219646569794,339.566597017035));
#8941=CARTESIAN_POINT('Ctrl Pts',(170.666950835149,-3.64065845225689,339.66672625614));
#8942=CARTESIAN_POINT('Ctrl Pts',(170.659552165394,-3.51505506497624,339.762053891506));
#8943=CARTESIAN_POINT('Ctrl Pts',(170.652153495639,-3.3858068480569,339.852240982283));
#8944=CARTESIAN_POINT('Ctrl Pts',(170.644756046435,-3.25657995308031,339.942413194991));
#8945=CARTESIAN_POINT('Ctrl Pts',(170.637358597231,-3.12370972758653,340.027446332818));
#8946=CARTESIAN_POINT('Ctrl Pts',(170.629961148028,-2.98764778617967,340.107043300016));
#8947=CARTESIAN_POINT('Ctrl Pts',(170.622564019564,-2.85159174418108,340.186636816028));
#8948=CARTESIAN_POINT('Ctrl Pts',(170.615166891101,-2.71234458356617,340.260794441613));
#8949=CARTESIAN_POINT('Ctrl Pts',(170.607769762637,-2.5703845068228,340.329263931312));
#8950=CARTESIAN_POINT('Ctrl Pts',(170.6003714952,-2.42840257177149,340.397743963603));
#8951=CARTESIAN_POINT('Ctrl Pts',(170.592973227764,-2.28370722502833,340.460533953971));
#8952=CARTESIAN_POINT('Ctrl Pts',(170.585574960327,-2.13679858804349,340.517428962536));
#8953=CARTESIAN_POINT('Ctrl Pts',(170.578174093801,-1.98983834050946,340.574343958916));
#8954=CARTESIAN_POINT('Ctrl Pts',(170.570773227276,-1.84066360243279,340.625359715499));
#8955=CARTESIAN_POINT('Ctrl Pts',(170.56337236075,-1.68979151587125,340.670320554906));
#8956=CARTESIAN_POINT('Ctrl Pts',(170.555963367365,-1.53875375733493,340.715330765613));
#8957=CARTESIAN_POINT('Ctrl Pts',(170.54855437398,-1.38601528598452,340.754272674328));
#8958=CARTESIAN_POINT('Ctrl Pts',(170.541145380596,-1.23210606479509,340.787041144453));
#8959=CARTESIAN_POINT('Ctrl Pts',(170.533731823015,-1.07810203021669,340.819829801086));
#8960=CARTESIAN_POINT('Ctrl Pts',(170.526318265435,-0.922926175652067,340.846437378122));
#8961=CARTESIAN_POINT('Ctrl Pts',(170.518904707855,-0.76711501892549,340.866810471648));
#8962=CARTESIAN_POINT('Ctrl Pts',(170.511480595718,-0.611082036491973,340.887212570003));
#8963=CARTESIAN_POINT('Ctrl Pts',(170.504056483582,-0.454412316186971,340.901362424364));
#8964=CARTESIAN_POINT('Ctrl Pts',(170.496632371445,-0.297644643054712,340.909258686922));
#8965=CARTESIAN_POINT('Ctrl Pts',(170.49277524629,-0.216197525288533,340.913361113229));
#8966=CARTESIAN_POINT('Ctrl Pts',(170.488918121135,-0.134723932638635,340.915776415404));
#8967=CARTESIAN_POINT('Ctrl Pts',(170.48506099598,-0.053298908672496,340.916509933131));
#8968=CARTESIAN_POINT('Ctrl Pts',(170.477637018542,0.103423395257105,340.917921766772));
#8969=CARTESIAN_POINT('Ctrl Pts',(170.470213041104,0.260438258282484,340.913104309305));
#8970=CARTESIAN_POINT('Ctrl Pts',(170.462789063666,0.417209698739794,340.902022249177));
#8971=CARTESIAN_POINT('Ctrl Pts',(170.455373847639,0.57379612530983,340.890953267547));
#8972=CARTESIAN_POINT('Ctrl Pts',(170.447958631611,0.730139332475785,340.873634425546));
#8973=CARTESIAN_POINT('Ctrl Pts',(170.440543415583,0.885701370265841,340.850082362259));
#8974=CARTESIAN_POINT('Ctrl Pts',(170.433135334439,1.04111372704623,340.826552960648));
#8975=CARTESIAN_POINT('Ctrl Pts',(170.425727253295,1.19574604428049,340.796802333297));
#8976=CARTESIAN_POINT('Ctrl Pts',(170.418319172151,1.34906364086855,340.760899049227));
#8977=CARTESIAN_POINT('Ctrl Pts',(170.410916604977,1.50226712036992,340.725022488627));
#8978=CARTESIAN_POINT('Ctrl Pts',(170.403514037803,1.65415746587748,340.683002474559));
#8979=CARTESIAN_POINT('Ctrl Pts',(170.396111470629,1.8042084733272,340.634958948145));
#8980=CARTESIAN_POINT('Ctrl Pts',(170.388712800874,1.95418047957709,340.586940716436));
#8981=CARTESIAN_POINT('Ctrl Pts',(170.38131413112,2.10231472186053,340.532905401836));
#8982=CARTESIAN_POINT('Ctrl Pts',(170.373915461365,2.24809859698889,340.473023228593));
#8983=CARTESIAN_POINT('Ctrl Pts',(170.366518012161,2.39385842230469,340.413150934049));
#8984=CARTESIAN_POINT('Ctrl Pts',(170.359120562957,2.53726830511264,340.347433836847));
#8985=CARTESIAN_POINT('Ctrl Pts',(170.351723113753,2.67783401668396,340.276090933787));
#8986=CARTESIAN_POINT('Ctrl Pts',(170.344325985289,2.81839363357107,340.204751124031));
#8987=CARTESIAN_POINT('Ctrl Pts',(170.336928856826,2.95610899161856,340.12778616233));
#8988=CARTESIAN_POINT('Ctrl Pts',(170.329531728362,3.09050918943231,340.045461674865));
#8989=CARTESIAN_POINT('Ctrl Pts',(170.322133460926,3.22493008152138,339.963124511485));
#8990=CARTESIAN_POINT('Ctrl Pts',(170.314735193489,3.3560344787274,339.875426374145));
#8991=CARTESIAN_POINT('Ctrl Pts',(170.307336926053,3.48337939831982,339.782676920916));
#8992=CARTESIAN_POINT('Ctrl Pts',(170.299936059527,3.61076905552088,339.689894883828));
#8993=CARTESIAN_POINT('Ctrl Pts',(170.292535193001,3.73439630402208,339.592058217247));
#8994=CARTESIAN_POINT('Ctrl Pts',(170.285134326476,3.85385037615274,339.489517550999));
#8995=CARTESIAN_POINT('Ctrl Pts',(170.277725333091,3.97343562027562,339.386864285295));
#8996=CARTESIAN_POINT('Ctrl Pts',(170.270316339706,4.088838253083,339.279496947496));
#8997=CARTESIAN_POINT('Ctrl Pts',(170.262907346321,4.19968306959087,339.167804299327));
#8998=CARTESIAN_POINT('Ctrl Pts',(170.255493788741,4.31059617032909,339.056042844635));
#8999=CARTESIAN_POINT('Ctrl Pts',(170.248080231161,4.41694560839942,338.939951044676));
#9000=CARTESIAN_POINT('Ctrl Pts',(170.240666673581,4.51839613473388,338.819951168814));
#9001=CARTESIAN_POINT('Ctrl Pts',(170.233242561444,4.61999109446562,338.69978045116));
#9002=CARTESIAN_POINT('Ctrl Pts',(170.225818449307,4.71667298423562,338.575690839066));
#9003=CARTESIAN_POINT('Ctrl Pts',(170.218394337171,4.80814910313857,338.448134678995));
#9004=CARTESIAN_POINT('Ctrl Pts',(170.214537212016,4.85567462979866,338.381864118341));
#9005=CARTESIAN_POINT('Ctrl Pts',(170.210680086861,4.90179574486097,338.314658294717));
#9006=CARTESIAN_POINT('Ctrl Pts',(170.206822961706,4.94647632820009,338.24658320347));
#9007=CARTESIAN_POINT('Ctrl Pts',(170.199398984268,5.03247500060989,338.115556098766));
#9008=CARTESIAN_POINT('Ctrl Pts',(170.19197500683,5.11339364974403,337.980911948022));
#9009=CARTESIAN_POINT('Ctrl Pts',(170.184551029392,5.18891253093172,337.843082360545));
#9010=CARTESIAN_POINT('Ctrl Pts',(170.177135813365,5.26434228847718,337.705415432718));
#9011=CARTESIAN_POINT('Ctrl Pts',(170.169720597337,5.33438478512638,337.564570875215));
#9012=CARTESIAN_POINT('Ctrl Pts',(170.162305381309,5.39876289744299,337.421010066004));
#9013=CARTESIAN_POINT('Ctrl Pts',(170.154897300165,5.46307906546404,337.277587390281));
#9014=CARTESIAN_POINT('Ctrl Pts',(170.147489219021,5.52174154787887,337.131454004233));
#9015=CARTESIAN_POINT('Ctrl Pts',(170.140081137877,5.57451865921723,336.983096639233));
#9016=CARTESIAN_POINT('Ctrl Pts',(170.132678570703,5.62725648758775,336.834849699331));
#9017=CARTESIAN_POINT('Ctrl Pts',(170.125276003529,5.67411754272069,336.684382426635));
#9018=CARTESIAN_POINT('Ctrl Pts',(170.117873436355,5.71491792645063,336.532202224393));
#9019=CARTESIAN_POINT('Ctrl Pts',(170.1104747666,5.75569682895688,336.380102144361));
#9020=CARTESIAN_POINT('Ctrl Pts',(170.103076096845,5.79042131855724,336.226291290444));
#9021=CARTESIAN_POINT('Ctrl Pts',(170.095677427091,5.8189571414556,336.071292839705));
#9022=CARTESIAN_POINT('Ctrl Pts',(170.088279977887,5.84748825682925,335.916319958898));
#9023=CARTESIAN_POINT('Ctrl Pts',(170.080882528683,5.86983266422436,335.760160236787));
#9024=CARTESIAN_POINT('Ctrl Pts',(170.073485079479,5.88590706719703,335.603347792587));
#9025=CARTESIAN_POINT('Ctrl Pts',(170.066087951015,5.9019807732116,335.446542147502));
#9026=CARTESIAN_POINT('Ctrl Pts',(170.058690822552,5.91178497728654,335.289084207867));
#9027=CARTESIAN_POINT('Ctrl Pts',(170.051293694088,5.91528821838032,335.131513710277));
#9028=CARTESIAN_POINT('Ctrl Pts',(170.043895426652,5.9187919988858,334.973918950764));
#9029=CARTESIAN_POINT('Ctrl Pts',(170.036497159215,5.91599287633608,334.816211971931));
#9030=CARTESIAN_POINT('Ctrl Pts',(170.029098891778,5.90691152543361,334.658932861155));
#9031=CARTESIAN_POINT('Ctrl Pts',(170.021698025253,5.89782698415703,334.501598496573));
#9032=CARTESIAN_POINT('Ctrl Pts',(170.014297158727,5.88245584186873,334.344692671681));
#9033=CARTESIAN_POINT('Ctrl Pts',(170.006896292201,5.86087066071359,334.188750555694));
#9034=CARTESIAN_POINT('Ctrl Pts',(169.999487298816,5.83926177696606,334.032637200356));
#9035=CARTESIAN_POINT('Ctrl Pts',(169.992078305431,5.8114252784424,333.877490037201));
#9036=CARTESIAN_POINT('Ctrl Pts',(169.984669312047,5.77748503822549,333.723834965382));
#9037=CARTESIAN_POINT('Ctrl Pts',(169.977255754466,5.74352388964973,333.570085236738));
#9038=CARTESIAN_POINT('Ctrl Pts',(169.969842196886,5.70345160162266,333.417829791094));
#9039=CARTESIAN_POINT('Ctrl Pts',(169.962428639306,5.65744184695399,333.267579060726));
#9040=CARTESIAN_POINT('Ctrl Pts',(169.955004527169,5.61136658897657,333.117114420937));
#9041=CARTESIAN_POINT('Ctrl Pts',(169.947580415032,5.55933710499126,332.968660547848));
#9042=CARTESIAN_POINT('Ctrl Pts',(169.940156302896,5.50157538553221,332.822708370519));
#9043=CARTESIAN_POINT('Ctrl Pts',(169.936299177741,5.47156584675026,332.746880338271));
#9044=CARTESIAN_POINT('Ctrl Pts',(169.932442052587,5.4400098176835,332.671727181239));
#9045=CARTESIAN_POINT('Ctrl Pts',(169.928584927432,5.40694324855453,332.597314987475));
#9046=CARTESIAN_POINT('Ctrl Pts',(169.921160949994,5.34329857711213,332.454090584456));
#9047=CARTESIAN_POINT('Ctrl Pts',(169.913736972556,5.27386316240172,332.313180690228));
#9048=CARTESIAN_POINT('Ctrl Pts',(169.906312995118,5.19882692171055,332.17508775347));
#9049=CARTESIAN_POINT('Ctrl Pts',(169.898897779091,5.12387923507308,332.037157787153));
#9050=CARTESIAN_POINT('Ctrl Pts',(169.891482563063,5.04334405585587,331.902038485706));
#9051=CARTESIAN_POINT('Ctrl Pts',(169.884067347035,4.95745939924524,331.770212566231));
#9052=CARTESIAN_POINT('Ctrl Pts',(169.876659265891,4.87165738041864,331.638513488991));
#9053=CARTESIAN_POINT('Ctrl Pts',(169.869251184747,4.78051633375831,331.510101795697));
#9054=CARTESIAN_POINT('Ctrl Pts',(169.861843103603,4.68432018376019,331.385435713877));
#9055=CARTESIAN_POINT('Ctrl Pts',(169.854440536429,4.5881956343136,331.260862423299));
#9056=CARTESIAN_POINT('Ctrl Pts',(169.847037969255,4.48702370044481,331.140029487235));
#9057=CARTESIAN_POINT('Ctrl Pts',(169.839635402081,4.38113155051904,331.023366134587));
#9058=CARTESIAN_POINT('Ctrl Pts',(169.832236732326,4.27529515234752,330.906764204685));
#9059=CARTESIAN_POINT('Ctrl Pts',(169.824838062572,4.16474373769147,330.794327761846));
#9060=CARTESIAN_POINT('Ctrl Pts',(169.817439392817,4.0498446048744,330.686452824082));
#9061=CARTESIAN_POINT('Ctrl Pts',(169.810041943613,3.93496442684627,330.578595682333));
#9062=CARTESIAN_POINT('Ctrl Pts',(169.802644494409,3.81573822596517,330.47529880738));
#9063=CARTESIAN_POINT('Ctrl Pts',(169.795247045205,3.69257007798922,330.376921287536));
#9064=CARTESIAN_POINT('Ctrl Pts',(169.787849916742,3.56940727036963,330.278548033169));
#9065=CARTESIAN_POINT('Ctrl Pts',(169.780452788278,3.44230314710271,330.185093942728));
#9066=CARTESIAN_POINT('Ctrl Pts',(169.773055659815,3.31169455883302,330.096877554915));
#9067=CARTESIAN_POINT('Ctrl Pts',(169.765657392378,3.18106586010079,330.00864758398));
#9068=CARTESIAN_POINT('Ctrl Pts',(169.758259124941,3.04693193124432,329.925657130378));
#9069=CARTESIAN_POINT('Ctrl Pts',(169.750860857505,2.9097581315298,329.84818108058));
#9070=CARTESIAN_POINT('Ctrl Pts',(169.743459990979,2.77253614121665,329.77067781263));
#9071=CARTESIAN_POINT('Ctrl Pts',(169.736059124453,2.63227247853844,329.698692989006));
#9072=CARTESIAN_POINT('Ctrl Pts',(169.728658257927,2.48945644624628,329.632455201422));
#9073=CARTESIAN_POINT('Ctrl Pts',(169.721249264543,2.34648358829712,329.566144678414));
#9074=CARTESIAN_POINT('Ctrl Pts',(169.713840271158,2.20095310227184,329.505593951563));
#9075=CARTESIAN_POINT('Ctrl Pts',(169.706431277773,2.05337426282041,329.450983447557));
#9076=CARTESIAN_POINT('Ctrl Pts',(169.699017720193,1.90570450971329,329.396339301597));
#9077=CARTESIAN_POINT('Ctrl Pts',(169.691604162613,1.75598424284574,329.34764278545));
#9078=CARTESIAN_POINT('Ctrl Pts',(169.684190605032,1.60473667993107,329.305024078138));
#9079=CARTESIAN_POINT('Ctrl Pts',(169.676766492896,1.45327378842125,329.262344695295));
#9080=CARTESIAN_POINT('Ctrl Pts',(169.669342380759,1.30027962018063,329.225760489368));
#9081=CARTESIAN_POINT('Ctrl Pts',(169.661918268622,1.14628713974621,329.195350453666));
#9082=CARTESIAN_POINT('Ctrl Pts',(169.658061143468,1.06628184632145,329.179551215791));
#9083=CARTESIAN_POINT('Ctrl Pts',(169.654204018313,0.986007175232782,329.165417668293));
#9084=CARTESIAN_POINT('Ctrl Pts',(169.650346893158,0.905538156062171,329.152955343901));
#9085=CARTESIAN_POINT('Ctrl Pts',(169.64292291572,0.750655916356401,329.128968563228));
#9086=CARTESIAN_POINT('Ctrl Pts',(169.635498938282,0.594586293016063,329.111103855623));
#9087=CARTESIAN_POINT('Ctrl Pts',(169.628074960844,0.437854580995084,329.099473419397));
#9088=CARTESIAN_POINT('Ctrl Pts',(169.620659744817,0.281307835975972,329.087856708836));
#9089=CARTESIAN_POINT('Ctrl Pts',(169.613244528789,0.124100926162767,329.082459652025));
#9090=CARTESIAN_POINT('Ctrl Pts',(169.605829312761,-0.0332314176589032,
329.08334332284));
#9091=CARTESIAN_POINT('Ctrl Pts',(169.598421231617,-0.190412377091678,329.084226143392));
#9092=CARTESIAN_POINT('Ctrl Pts',(169.591013150473,-0.347718159546598,329.091377658434));
#9093=CARTESIAN_POINT('Ctrl Pts',(169.583605069329,-0.504609783880745,329.104807083011));
#9094=CARTESIAN_POINT('Ctrl Pts',(169.576202502155,-0.661384630912652,329.118226511823));
#9095=CARTESIAN_POINT('Ctrl Pts',(169.568799934981,-0.817745563366454,329.137914514325));
#9096=CARTESIAN_POINT('Ctrl Pts',(169.561397367807,-0.973154583926014,329.163828248048));
#9097=CARTESIAN_POINT('Ctrl Pts',(169.553998698052,-1.12848178231773,329.189728338304));
#9098=CARTESIAN_POINT('Ctrl Pts',(169.546600028298,-1.28285769973831,329.221847570577));
#9099=CARTESIAN_POINT('Ctrl Pts',(169.539201358543,-1.43575054999479,329.260091383943));
#9100=CARTESIAN_POINT('Ctrl Pts',(169.531803909339,-1.58861817767728,329.298328888266));
#9101=CARTESIAN_POINT('Ctrl Pts',(169.524406460135,-1.74000286206222,329.342688877956));
#9102=CARTESIAN_POINT('Ctrl Pts',(169.517009010931,-1.88938396954852,329.393025880378));
#9103=CARTESIAN_POINT('Ctrl Pts',(169.509611882467,-2.03875860013019,329.443360700275));
#9104=CARTESIAN_POINT('Ctrl Pts',(169.502214754004,-2.18612947287106,329.499671898445));
#9105=CARTESIAN_POINT('Ctrl Pts',(169.49481762554,-2.33099231682914,329.561764497433));
#9106=CARTESIAN_POINT('Ctrl Pts',(169.487419358104,-2.47587746604872,329.62386665713));
#9107=CARTESIAN_POINT('Ctrl Pts',(169.480021090667,-2.61825347451373,329.691751843092));
#9108=CARTESIAN_POINT('Ctrl Pts',(169.472622823231,-2.75763735172414,329.765177481626));
#9109=CARTESIAN_POINT('Ctrl Pts',(169.465221956705,-2.8970701959568,329.838628915359));
#9110=CARTESIAN_POINT('Ctrl Pts',(169.457821090179,-3.03350848607352,329.917624503148));
#9111=CARTESIAN_POINT('Ctrl Pts',(169.450420223653,-3.16649520462957,330.001876483963));
#9112=CARTESIAN_POINT('Ctrl Pts',(169.443011230269,-3.29962795531663,330.086220981509));
#9113=CARTESIAN_POINT('Ctrl Pts',(169.435602236884,-3.4293012498449,330.175833199265));
#9114=CARTESIAN_POINT('Ctrl Pts',(169.428193243499,-3.55508776582668,330.270382516549));
#9115=CARTESIAN_POINT('Ctrl Pts',(169.420779685919,-3.68095177064158,330.364990079473));
#9116=CARTESIAN_POINT('Ctrl Pts',(169.413366128339,-3.80292393731364,330.464540566932));
#9117=CARTESIAN_POINT('Ctrl Pts',(169.405952570758,-3.92061165239879,330.568664441325));
#9118=CARTESIAN_POINT('Ctrl Pts',(169.398528458622,-4.03846691749119,330.672936555116));
#9119=CARTESIAN_POINT('Ctrl Pts',(169.391104346485,-4.1520252799831,330.781794802148));
#9120=CARTESIAN_POINT('Ctrl Pts',(169.383680234348,-4.26093189502371,330.894833748985));
#9121=CARTESIAN_POINT('Ctrl Pts',(169.379823109194,-4.31751326618876,330.953562032889));
#9122=CARTESIAN_POINT('Ctrl Pts',(169.375965984039,-4.3728396984905,331.013418242858));
#9123=CARTESIAN_POINT('Ctrl Pts',(169.372108858885,-4.42686593652754,331.074342278992));
#9124=CARTESIAN_POINT('Ctrl Pts',(169.364751936199,-4.5299133721978,331.190546292493));
#9125=CARTESIAN_POINT('Ctrl Pts',(169.357395013513,-4.62855304767428,331.311003372299));
#9126=CARTESIAN_POINT('Ctrl Pts',(169.350038090827,-4.72240849342267,331.435341729738));
#9127=CARTESIAN_POINT('Ctrl Pts',(169.342538670572,-4.81808184231687,331.562088419366));
#9128=CARTESIAN_POINT('Ctrl Pts',(169.335039250317,-4.90878340356712,331.692868053281));
#9129=CARTESIAN_POINT('Ctrl Pts',(169.327539830062,-4.99415331427621,331.827246742023));
#9130=CARTESIAN_POINT('Ctrl Pts',(169.320200871848,-5.07769659977142,331.958750184685));
#9131=CARTESIAN_POINT('Ctrl Pts',(169.312861913634,-5.15613383886759,332.093699900124));
#9132=CARTESIAN_POINT('Ctrl Pts',(169.30552295542,-5.22916830256277,332.231655833179));
#9133=CARTESIAN_POINT('Ctrl Pts',(169.298188967279,-5.30215330602424,332.369518340029));
#9134=CARTESIAN_POINT('Ctrl Pts',(169.290854979137,-5.36974263697946,332.51038267876));
#9135=CARTESIAN_POINT('Ctrl Pts',(169.283520990996,-5.43168370675522,332.653781196847));
#9136=CARTESIAN_POINT('Ctrl Pts',(169.276190456817,-5.49359560520898,332.797112180996));
#9137=CARTESIAN_POINT('Ctrl Pts',(169.268859922638,-5.54986438627201,332.942974620463));
#9138=CARTESIAN_POINT('Ctrl Pts',(169.261529388459,-5.60028423835156,333.090877947283));
#9139=CARTESIAN_POINT('Ctrl Pts',(169.253906273146,-5.65271648095285,333.244684489617));
#9140=CARTESIAN_POINT('Ctrl Pts',(169.246283157833,-5.69882306887463,333.400697811828));
#9141=CARTESIAN_POINT('Ctrl Pts',(169.23866004252,-5.73842853454316,333.558345215927));
#9142=CARTESIAN_POINT('Ctrl Pts',(169.231330355198,-5.77650951163725,333.70992447609));
#9143=CARTESIAN_POINT('Ctrl Pts',(169.224000667875,-5.80858045972651,333.863013962719));
#9144=CARTESIAN_POINT('Ctrl Pts',(169.216670980552,-5.8345369607319,334.017091552405));
#9145=CARTESIAN_POINT('Ctrl Pts',(169.209340465971,-5.86049639129298,334.171186531911));
#9146=CARTESIAN_POINT('Ctrl Pts',(169.20200995139,-5.88033994501261,334.326269460021));
#9147=CARTESIAN_POINT('Ctrl Pts',(169.19467943681,-5.89401481477528,334.48181091703));
#9148=CARTESIAN_POINT('Ctrl Pts',(169.187344914374,-5.90769716107801,334.637437414112));
#9149=CARTESIAN_POINT('Ctrl Pts',(169.180010391939,-5.91520406817465,334.793522560859));
#9150=CARTESIAN_POINT('Ctrl Pts',(169.172675869504,-5.91653478056043,334.949534636445));
#9151=CARTESIAN_POINT('Ctrl Pts',(169.171801247904,-5.9166934643475,334.968138646784));
#9152=CARTESIAN_POINT('Ctrl Pts',(169.170926626303,-5.91676438408337,334.986741620344));
#9153=CARTESIAN_POINT('Ctrl Pts',(169.170052004703,-5.91674758786482,335.005342658123));
#9154=CARTESIAN_POINT('',(167.420052004703,-5.92202873839451,334.999419944072));
#9155=CARTESIAN_POINT('Ctrl Pts',(169.170050945661,-5.91432982443071,335.005362988975));
#9156=CARTESIAN_POINT('Ctrl Pts',(169.144657571978,-5.91904404249479,335.545201194357));
#9157=CARTESIAN_POINT('Ctrl Pts',(169.026518186868,-5.60357054579488,338.0513146166));
#9158=CARTESIAN_POINT('Ctrl Pts',(168.815632790337,-2.05622536433816,341.687642347814));
#9159=CARTESIAN_POINT('Ctrl Pts',(168.537394756062,4.51103959403896,340.348190787755));
#9160=CARTESIAN_POINT('Ctrl Pts',(168.25915672179,6.93859009980183,334.100783480941));
#9161=CARTESIAN_POINT('Ctrl Pts',(167.980918687515,2.99869888439871,328.678573901253));
#9162=CARTESIAN_POINT('Ctrl Pts',(167.702680653241,-3.69305403649433,329.057443748289));
#9163=CARTESIAN_POINT('Ctrl Pts',(167.515725092304,-5.9122207605932,332.976298931997));
#9164=CARTESIAN_POINT('Ctrl Pts',(167.421515542791,-5.92647291942922,334.968470644554));
#9165=CARTESIAN_POINT('Ctrl Pts',(167.420052004703,-5.92642976230421,334.999419512997));
#9166=CARTESIAN_POINT('',(165.670052025949,-5.91423241416373,334.994968760502));
#9167=CARTESIAN_POINT('Ctrl Pts',(167.420052004703,-5.91674997161742,334.999420461121));
#9168=CARTESIAN_POINT('Ctrl Pts',(167.412648369967,-5.91676528161425,335.155726494585));
#9169=CARTESIAN_POINT('Ctrl Pts',(167.40524473523,-5.91058248256132,335.312274754108));
#9170=CARTESIAN_POINT('Ctrl Pts',(167.397841100494,-5.89816995282945,335.468531503786));
#9171=CARTESIAN_POINT('Ctrl Pts',(167.390446191951,-5.88577205295576,335.624604083585));
#9172=CARTESIAN_POINT('Ctrl Pts',(167.383051283407,-5.86715906595222,335.780385466768));
#9173=CARTESIAN_POINT('Ctrl Pts',(167.375656374863,-5.84235133423688,335.935340285586));
#9174=CARTESIAN_POINT('Ctrl Pts',(167.368268546698,-5.81756735509657,336.090146740338));
#9175=CARTESIAN_POINT('Ctrl Pts',(167.360880718532,-5.7866004971388,336.244127837844));
#9176=CARTESIAN_POINT('Ctrl Pts',(167.353492890367,-5.74952301007913,336.396751845916));
#9177=CARTESIAN_POINT('Ctrl Pts',(167.346110502519,-5.71247282648276,336.549263463308));
#9178=CARTESIAN_POINT('Ctrl Pts',(167.33872811467,-5.66932106103354,336.700419617601));
#9179=CARTESIAN_POINT('Ctrl Pts',(167.331345726822,-5.62019127066978,336.8496974465));
#9180=CARTESIAN_POINT('Ctrl Pts',(167.323631512567,-5.56885317560087,337.005685072641));
#9181=CARTESIAN_POINT('Ctrl Pts',(167.315917298312,-5.51098725448226,337.159621185502));
#9182=CARTESIAN_POINT('Ctrl Pts',(167.308203084056,-5.44679332156382,337.310924722848));
#9183=CARTESIAN_POINT('Ctrl Pts',(167.300825635713,-5.38540179050894,337.455623067213));
#9184=CARTESIAN_POINT('Ctrl Pts',(167.293448187371,-5.31822320842122,337.597913440029));
#9185=CARTESIAN_POINT('Ctrl Pts',(167.286070739028,-5.24548207423519,337.737306773341));
#9186=CARTESIAN_POINT('Ctrl Pts',(167.278693424878,-5.17274226317604,337.876697571153));
#9187=CARTESIAN_POINT('Ctrl Pts',(167.271316110727,-5.09444027467716,338.013191101186));
#9188=CARTESIAN_POINT('Ctrl Pts',(167.263938796577,-5.01084690302941,338.146322277978));
#9189=CARTESIAN_POINT('Ctrl Pts',(167.256560139632,-4.92723831599127,338.279477686869));
#9190=CARTESIAN_POINT('Ctrl Pts',(167.249181482687,-4.83833662812618,338.409269206145));
#9191=CARTESIAN_POINT('Ctrl Pts',(167.241802825742,-4.74445624796787,338.535260312002));
#9192=CARTESIAN_POINT('Ctrl Pts',(167.234421348463,-4.65053998403919,338.661299575269));
#9193=CARTESIAN_POINT('Ctrl Pts',(167.227039871184,-4.55164146360955,338.783535232465));
#9194=CARTESIAN_POINT('Ctrl Pts',(167.219658393905,-4.44811556479037,338.901563594864));
#9195=CARTESIAN_POINT('Ctrl Pts',(167.212268753758,-4.34447518098295,339.019722479923));
#9196=CARTESIAN_POINT('Ctrl Pts',(167.20487911361,-4.2361974492157,339.133664498197));
#9197=CARTESIAN_POINT('Ctrl Pts',(167.197489473462,-4.12367476806568,339.24302215051));
#9198=CARTESIAN_POINT('Ctrl Pts',(167.190095037495,-4.01107906057267,339.352450775087));
#9199=CARTESIAN_POINT('Ctrl Pts',(167.182700601529,-3.89423319378537,339.457288856403));
#9200=CARTESIAN_POINT('Ctrl Pts',(167.175306165562,-3.77356239496176,339.557209388851));
#9201=CARTESIAN_POINT('Ctrl Pts',(167.167901612578,-3.65272649517612,339.657266631888));
#9202=CARTESIAN_POINT('Ctrl Pts',(167.160497059595,-3.52805551274428,339.752392666968));
#9203=CARTESIAN_POINT('Ctrl Pts',(167.153092506612,-3.40000387323542,339.842303607219));
#9204=CARTESIAN_POINT('Ctrl Pts',(167.150796532639,-3.36029813648877,339.870182829523));
#9205=CARTESIAN_POINT('Ctrl Pts',(167.148500558666,-3.32026753858626,339.897560968234));
#9206=CARTESIAN_POINT('Ctrl Pts',(167.146204584693,-3.27992608558425,339.924430468146));
#9207=CARTESIAN_POINT('Ctrl Pts',(167.138780607255,-3.14948295319161,340.01131235944));
#9208=CARTESIAN_POINT('Ctrl Pts',(167.131356629817,-3.01538853812546,340.093138779107));
#9209=CARTESIAN_POINT('Ctrl Pts',(167.123932652379,-2.8780722797421,340.169587073943));
#9210=CARTESIAN_POINT('Ctrl Pts',(167.116517436352,-2.74091807520394,340.245945148289));
#9211=CARTESIAN_POINT('Ctrl Pts',(167.109102220324,-2.60054991871874,340.316937551828));
#9212=CARTESIAN_POINT('Ctrl Pts',(167.101687004296,-2.45742730556294,340.38228405051));
#9213=CARTESIAN_POINT('Ctrl Pts',(167.094278923152,-2.31444240426478,340.44756767312));
#9214=CARTESIAN_POINT('Ctrl Pts',(167.086870842008,-2.16870865982743,340.50721605192));
#9215=CARTESIAN_POINT('Ctrl Pts',(167.079462760864,-2.02071122731929,340.560994218509));
#9216=CARTESIAN_POINT('Ctrl Pts',(167.07206019369,-1.87282395200341,340.614732357026));
#9217=CARTESIAN_POINT('Ctrl Pts',(167.064657626516,-1.72267669277552,340.662608856343));
#9218=CARTESIAN_POINT('Ctrl Pts',(167.057255059342,-1.5707755989397,340.704436394621));
#9219=CARTESIAN_POINT('Ctrl Pts',(167.049856389587,-1.41895448036626,340.746241910883));
#9220=CARTESIAN_POINT('Ctrl Pts',(167.042457719833,-1.26538172507636,340.782004709896));
#9221=CARTESIAN_POINT('Ctrl Pts',(167.035059050078,-1.1105795912168,340.811587006496));
#9222=CARTESIAN_POINT('Ctrl Pts',(167.027661600874,-0.95580299490186,340.841164422935));
#9223=CARTESIAN_POINT('Ctrl Pts',(167.02026415167,-0.799797788749643,340.864563290536));
#9224=CARTESIAN_POINT('Ctrl Pts',(167.012866702466,-0.64309751706047,340.881696706398));
#9225=CARTESIAN_POINT('Ctrl Pts',(167.005469574002,-0.486404039621832,340.898829379385));
#9226=CARTESIAN_POINT('Ctrl Pts',(166.998072445539,-0.329015927568422,340.909697100217));
#9227=CARTESIAN_POINT('Ctrl Pts',(166.990675317076,-0.171472692638845,340.914264762266));
#9228=CARTESIAN_POINT('Ctrl Pts',(166.983277049639,-0.0139051999841216,
340.91883312762));
#9229=CARTESIAN_POINT('Ctrl Pts',(166.975878782202,0.143817090027833,340.917099491874));
#9230=CARTESIAN_POINT('Ctrl Pts',(166.968480514766,0.301153962671562,340.909080880583));
#9231=CARTESIAN_POINT('Ctrl Pts',(166.96107964824,0.458546109413887,340.901059452269));
#9232=CARTESIAN_POINT('Ctrl Pts',(166.953678781714,0.615552196711758,340.886748671313));
#9233=CARTESIAN_POINT('Ctrl Pts',(166.946277915188,0.771636577353052,340.866217482756));
#9234=CARTESIAN_POINT('Ctrl Pts',(166.938868921804,0.927892353566265,340.845663748991));
#9235=CARTESIAN_POINT('Ctrl Pts',(166.931459928419,1.0832240316166,340.818876015248));
#9236=CARTESIAN_POINT('Ctrl Pts',(166.924050935034,1.23710488750165,340.785974598961));
#9237=CARTESIAN_POINT('Ctrl Pts',(166.916637377454,1.39108053930175,340.753052914266));
#9238=CARTESIAN_POINT('Ctrl Pts',(166.909223819874,1.54360322729965,340.714010134631));
#9239=CARTESIAN_POINT('Ctrl Pts',(166.901810262293,1.69416135758378,340.66901648057));
#9240=CARTESIAN_POINT('Ctrl Pts',(166.894386150157,1.8449338349298,340.623958769804));
#9241=CARTESIAN_POINT('Ctrl Pts',(166.88696203802,1.99373581649814,340.572933384746));
#9242=CARTESIAN_POINT('Ctrl Pts',(166.879537925883,2.14007488472642,340.516158994288));
#9243=CARTESIAN_POINT('Ctrl Pts',(166.875680800729,2.21610392237841,340.486662412671));
#9244=CARTESIAN_POINT('Ctrl Pts',(166.871823675574,2.29146854785813,340.455614816797));
#9245=CARTESIAN_POINT('Ctrl Pts',(166.867966550419,2.36610243175137,340.423051709597));
#9246=CARTESIAN_POINT('Ctrl Pts',(166.860542572981,2.50975353144761,340.360376073347));
#9247=CARTESIAN_POINT('Ctrl Pts',(166.853118595543,2.65112929576347,340.291894189819));
#9248=CARTESIAN_POINT('Ctrl Pts',(166.845694618105,2.78972600446066,340.217792577569));
#9249=CARTESIAN_POINT('Ctrl Pts',(166.838279402078,2.92815914818906,340.14377841637));
#9250=CARTESIAN_POINT('Ctrl Pts',(166.83086418605,3.06381943867884,340.064157902056));
#9251=CARTESIAN_POINT('Ctrl Pts',(166.823448970022,3.19622256187971,339.979165783284));
#9252=CARTESIAN_POINT('Ctrl Pts',(166.816040888878,3.32849828746126,339.894255443502));
#9253=CARTESIAN_POINT('Ctrl Pts',(166.808632807734,3.45752277305123,339.803983989103));
#9254=CARTESIAN_POINT('Ctrl Pts',(166.80122472659,3.58283588346338,339.708632242453));
#9255=CARTESIAN_POINT('Ctrl Pts',(166.793822159416,3.70805572103873,339.613351467849));
#9256=CARTESIAN_POINT('Ctrl Pts',(166.786419592242,3.82956938813069,339.512998155247));
#9257=CARTESIAN_POINT('Ctrl Pts',(166.779017025068,3.94694545537717,339.407896565798));
#9258=CARTESIAN_POINT('Ctrl Pts',(166.771618355314,4.0642597246369,339.302850311878));
#9259=CARTESIAN_POINT('Ctrl Pts',(166.764219685559,4.17744045518329,339.193061008239));
#9260=CARTESIAN_POINT('Ctrl Pts',(166.756821015804,4.28608915668034,339.078893269441));
#9261=CARTESIAN_POINT('Ctrl Pts',(166.7494235666,4.39471993451602,338.964744364773));
#9262=CARTESIAN_POINT('Ctrl Pts',(166.742026117396,4.49881991009974,338.84621872858));
#9263=CARTESIAN_POINT('Ctrl Pts',(166.734628668192,4.59802727349437,338.723718001501));
#9264=CARTESIAN_POINT('Ctrl Pts',(166.727231539729,4.69723033543055,338.60122258584));
#9265=CARTESIAN_POINT('Ctrl Pts',(166.719834411265,4.79154097209094,338.474752712019));
#9266=CARTESIAN_POINT('Ctrl Pts',(166.712437282802,4.88063770080368,338.344743068756));
#9267=CARTESIAN_POINT('Ctrl Pts',(166.705039015365,4.96974814818885,338.214713407254));
#9268=CARTESIAN_POINT('Ctrl Pts',(166.697640747929,5.05364287813316,338.081143198947));
#9269=CARTESIAN_POINT('Ctrl Pts',(166.690242480492,5.13204386660433,337.944495935427));
#9270=CARTESIAN_POINT('Ctrl Pts',(166.682841613966,5.21047239816723,337.807800666288));
#9271=CARTESIAN_POINT('Ctrl Pts',(166.67544074744,5.28340315999887,337.668026513174));
#9272=CARTESIAN_POINT('Ctrl Pts',(166.668039880915,5.35060426001229,337.525661223371));
#9273=CARTESIAN_POINT('Ctrl Pts',(166.66063088753,5.417879153258,337.383139602869));
#9274=CARTESIAN_POINT('Ctrl Pts',(166.653221894145,5.47941166038539,337.238021501133));
#9275=CARTESIAN_POINT('Ctrl Pts',(166.64581290076,5.5350179183095,337.09081496228));
#9276=CARTESIAN_POINT('Ctrl Pts',(166.63839934318,5.59065843160656,336.943517739121));
#9277=CARTESIAN_POINT('Ctrl Pts',(166.6309857856,5.64036530349625,336.79412986852));
#9278=CARTESIAN_POINT('Ctrl Pts',(166.62357222802,5.68400482321869,336.643173676799));
#9279=CARTESIAN_POINT('Ctrl Pts',(166.616148115883,5.72770647178675,336.492002571304));
#9280=CARTESIAN_POINT('Ctrl Pts',(166.608724003746,5.76532342739506,336.339259046761));
#9281=CARTESIAN_POINT('Ctrl Pts',(166.60129989161,5.79677309798291,336.185475521891));
#9282=CARTESIAN_POINT('Ctrl Pts',(166.597442766455,5.8131124680383,336.105578789292));
#9283=CARTESIAN_POINT('Ctrl Pts',(166.5935856413,5.82778800556544,336.025401432252));
#9284=CARTESIAN_POINT('Ctrl Pts',(166.589728516145,5.8407936710839,335.945018441263));
#9285=CARTESIAN_POINT('Ctrl Pts',(166.582304538707,5.86582624417931,335.790301783764));
#9286=CARTESIAN_POINT('Ctrl Pts',(166.574880561269,5.88474490553512,335.634356410765));
#9287=CARTESIAN_POINT('Ctrl Pts',(166.567456583831,5.89743391065884,335.477706847252));
#9288=CARTESIAN_POINT('Ctrl Pts',(166.560041367804,5.91010794084733,335.321242153793));
#9289=CARTESIAN_POINT('Ctrl Pts',(166.552626151776,5.9165669191014,335.164075292416));
#9290=CARTESIAN_POINT('Ctrl Pts',(166.545210935748,5.91674616045239,335.006740569106));
#9291=CARTESIAN_POINT('Ctrl Pts',(166.537802854604,5.91692522933826,334.849557232474));
#9292=CARTESIAN_POINT('Ctrl Pts',(166.53039477346,5.91083659005377,334.692206726175));
#9293=CARTESIAN_POINT('Ctrl Pts',(166.522986692316,5.8984673865637,334.535227956796));
#9294=CARTESIAN_POINT('Ctrl Pts',(166.515584125142,5.88610738969763,334.378366029581));
#9295=CARTESIAN_POINT('Ctrl Pts',(166.508181557968,5.86747616590226,334.22187565882));
#9296=CARTESIAN_POINT('Ctrl Pts',(166.500778990794,5.84261292211522,334.066295118984));
#9297=CARTESIAN_POINT('Ctrl Pts',(166.493380321039,5.81776276871761,333.910796491624));
#9298=CARTESIAN_POINT('Ctrl Pts',(166.485981651285,5.78668718864312,333.756207108795));
#9299=CARTESIAN_POINT('Ctrl Pts',(166.47858298153,5.74947714806621,333.603059383379));
#9300=CARTESIAN_POINT('Ctrl Pts',(166.471185532326,5.71227324599036,333.449936922583));
#9301=CARTESIAN_POINT('Ctrl Pts',(166.463788083122,5.66893697992537,333.298256009495));
#9302=CARTESIAN_POINT('Ctrl Pts',(166.456390633918,5.6196103019363,333.148538248607));
#9303=CARTESIAN_POINT('Ctrl Pts',(166.448993505454,5.57028576266609,332.998826979221));
#9304=CARTESIAN_POINT('Ctrl Pts',(166.441596376991,5.51497144469301,332.851079047259));
#9305=CARTESIAN_POINT('Ctrl Pts',(166.434199248527,5.45385891431485,332.705800029368));
#9306=CARTESIAN_POINT('Ctrl Pts',(166.426800981091,5.3927369741325,332.560498642134));
#9307=CARTESIAN_POINT('Ctrl Pts',(166.419402713654,5.32581518862284,332.417667269937));
#9308=CARTESIAN_POINT('Ctrl Pts',(166.412004446218,5.25333286299755,332.277790531012));
#9309=CARTESIAN_POINT('Ctrl Pts',(166.404603579692,5.18082507356891,332.137864651917));
#9310=CARTESIAN_POINT('Ctrl Pts',(166.397202713166,5.10275302625763,332.000895803894));
#9311=CARTESIAN_POINT('Ctrl Pts',(166.38980184664,5.01940138804739,331.867342937989));
#9312=CARTESIAN_POINT('Ctrl Pts',(166.382392853256,4.93595822176967,331.733643418269));
#9313=CARTESIAN_POINT('Ctrl Pts',(166.374983859871,4.84722408440145,331.603367688563));
#9314=CARTESIAN_POINT('Ctrl Pts',(166.367574866486,4.75352670221447,331.476945295084));
#9315=CARTESIAN_POINT('Ctrl Pts',(166.360161308906,4.65977159920789,331.350445021049));
#9316=CARTESIAN_POINT('Ctrl Pts',(166.352747751325,4.56104739232786,331.227803103371));
#9317=CARTESIAN_POINT('Ctrl Pts',(166.345334193745,4.45772095835694,331.109414643023));
#9318=CARTESIAN_POINT('Ctrl Pts',(166.337910081608,4.35424742029131,330.990857635028));
#9319=CARTESIAN_POINT('Ctrl Pts',(166.330485969472,4.2461588250031,330.876566448983));
#9320=CARTESIAN_POINT('Ctrl Pts',(166.323061857335,4.13385819944831,330.766898660633));
#9321=CARTESIAN_POINT('Ctrl Pts',(166.31920473218,4.07551350317672,330.709921829288));
#9322=CARTESIAN_POINT('Ctrl Pts',(166.315347607026,4.01603242857411,330.654192288226));
#9323=CARTESIAN_POINT('Ctrl Pts',(166.311490481871,3.95547476843586,330.599755697831));
#9324=CARTESIAN_POINT('Ctrl Pts',(166.304066504433,3.83891679208092,330.494979212057));
#9325=CARTESIAN_POINT('Ctrl Pts',(166.296642526995,3.71801697418941,330.394679116637));
#9326=CARTESIAN_POINT('Ctrl Pts',(166.289218549557,3.59315376302699,330.299236594154));
#9327=CARTESIAN_POINT('Ctrl Pts',(166.28180333353,3.46843790924056,330.203906708207));
#9328=CARTESIAN_POINT('Ctrl Pts',(166.274388117502,3.33976826625009,330.113423208673));
#9329=CARTESIAN_POINT('Ctrl Pts',(166.266972901475,3.20755913860955,330.028129634149));
#9330=CARTESIAN_POINT('Ctrl Pts',(166.25956482033,3.07547722192567,329.942918128674));
#9331=CARTESIAN_POINT('Ctrl Pts',(166.252156739186,2.93986291216941,329.862886807614));
#9332=CARTESIAN_POINT('Ctrl Pts',(166.244748658042,2.80116243025032,329.788338115164));
#9333=CARTESIAN_POINT('Ctrl Pts',(166.237346090868,2.66256518563315,329.713844910667));
#9334=CARTESIAN_POINT('Ctrl Pts',(166.229943523694,2.52088667003073,329.644826385202));
#9335=CARTESIAN_POINT('Ctrl Pts',(166.22254095652,2.37660074705245,329.581540860022));
#9336=CARTESIAN_POINT('Ctrl Pts',(166.215142286765,2.23239078998174,329.518288654395));
#9337=CARTESIAN_POINT('Ctrl Pts',(166.207743617011,2.08557650044486,329.460763587261));
#9338=CARTESIAN_POINT('Ctrl Pts',(166.200344947256,1.93665482281105,329.409177282387));
#9339=CARTESIAN_POINT('Ctrl Pts',(166.192947498052,1.78775771263016,329.357599487651));
#9340=CARTESIAN_POINT('Ctrl Pts',(166.185550048848,1.63675425664227,329.311958632802));
#9341=CARTESIAN_POINT('Ctrl Pts',(166.178152599644,1.48415990159975,329.272417617442));
#9342=CARTESIAN_POINT('Ctrl Pts',(166.17075547118,1.33157216278268,329.232878316512));
#9343=CARTESIAN_POINT('Ctrl Pts',(166.163358342717,1.17739402334233,329.199438422816));
#9344=CARTESIAN_POINT('Ctrl Pts',(166.155961214253,1.02215430098216,329.1722104407));
#9345=CARTESIAN_POINT('Ctrl Pts',(166.148562946817,0.866890675579753,329.144978266155));
#9346=CARTESIAN_POINT('Ctrl Pts',(166.14116467938,0.710565509414855,329.123959972145));
#9347=CARTESIAN_POINT('Ctrl Pts',(166.133766411944,0.553715830082504,329.109216576548));
#9348=CARTESIAN_POINT('Ctrl Pts',(166.126365545418,0.396811047807554,329.094468001441));
#9349=CARTESIAN_POINT('Ctrl Pts',(166.118964678892,0.239381756829181,329.085998748683));
#9350=CARTESIAN_POINT('Ctrl Pts',(166.111563812366,0.0819679485124542,329.08381780048));
#9351=CARTESIAN_POINT('Ctrl Pts',(166.104154818982,-0.0756187152145948,
329.081634457388));
#9352=CARTESIAN_POINT('Ctrl Pts',(166.096745825597,-0.233189488929145,329.085753213996));
#9353=CARTESIAN_POINT('Ctrl Pts',(166.089336832212,-0.390205806565071,329.096130930396));
#9354=CARTESIAN_POINT('Ctrl Pts',(166.081923274632,-0.547318851668759,329.106515039828));
#9355=CARTESIAN_POINT('Ctrl Pts',(166.074509717052,-0.703876389831103,329.123165752734));
#9356=CARTESIAN_POINT('Ctrl Pts',(166.067096159471,-0.859347634135345,329.14598836641));
#9357=CARTESIAN_POINT('Ctrl Pts',(166.059672047335,-1.01504022021867,329.168843472255));
#9358=CARTESIAN_POINT('Ctrl Pts',(166.052247935198,-1.16964305789237,329.197887959206));
#9359=CARTESIAN_POINT('Ctrl Pts',(166.044823823061,-1.32263735307258,329.232976418051));
#9360=CARTESIAN_POINT('Ctrl Pts',(166.040966697907,-1.40212404906893,329.251206285105));
#9361=CARTESIAN_POINT('Ctrl Pts',(166.037109572752,-1.48117683157777,329.271066737282));
#9362=CARTESIAN_POINT('Ctrl Pts',(166.033252447597,-1.5597249464937,329.292532203001));
#9363=CARTESIAN_POINT('Ctrl Pts',(166.025828470159,-1.71090993779083,329.333847723447));
#9364=CARTESIAN_POINT('Ctrl Pts',(166.018404492721,-1.86068025652888,329.381236822746));
#9365=CARTESIAN_POINT('Ctrl Pts',(166.010980515283,-2.00851055807154,329.434587535446));
#9366=CARTESIAN_POINT('Ctrl Pts',(166.003565299256,-2.15616639761601,329.487875286277));
#9367=CARTESIAN_POINT('Ctrl Pts',(165.996150083228,-2.30188642963945,329.547110520575));
#9368=CARTESIAN_POINT('Ctrl Pts',(165.9887348672,-2.44515756123928,329.612130749247));
#9369=CARTESIAN_POINT('Ctrl Pts',(165.981326786056,-2.58829083807782,329.677088415782));
#9370=CARTESIAN_POINT('Ctrl Pts',(165.973918704912,-2.72897956790627,329.747819842039));
#9371=CARTESIAN_POINT('Ctrl Pts',(165.966510623768,-2.86672794321283,329.824113461241));
#9372=CARTESIAN_POINT('Ctrl Pts',(165.959108056594,-3.00437378988889,329.90035029371));
#9373=CARTESIAN_POINT('Ctrl Pts',(165.95170548942,-3.13908331470249,329.982140895648));
#9374=CARTESIAN_POINT('Ctrl Pts',(165.944302922246,-3.27038285501261,330.069226577489));
#9375=CARTESIAN_POINT('Ctrl Pts',(165.936904252491,-3.40161326668806,330.156266409099));
#9376=CARTESIAN_POINT('Ctrl Pts',(165.929505582737,-3.52943695915461,330.248595562702));
#9377=CARTESIAN_POINT('Ctrl Pts',(165.922106912982,-3.65340704836094,330.34591066894));
#9378=CARTESIAN_POINT('Ctrl Pts',(165.914709463778,-3.77735668635163,330.443209721207));
#9379=CARTESIAN_POINT('Ctrl Pts',(165.907312014574,-3.89745368950972,330.545492863434));
#9380=CARTESIAN_POINT('Ctrl Pts',(165.89991456537,-4.01328213427224,330.652414799773));
#9381=CARTESIAN_POINT('Ctrl Pts',(165.892517436906,-4.12910555691527,330.759332100163));
#9382=CARTESIAN_POINT('Ctrl Pts',(165.885120308443,-4.24066051492431,330.870887541605));
#9383=CARTESIAN_POINT('Ctrl Pts',(165.877723179979,-4.34756622739132,330.986697312568));
#9384=CARTESIAN_POINT('Ctrl Pts',(165.870324912543,-4.45448840066969,331.102524915345));
#9385=CARTESIAN_POINT('Ctrl Pts',(165.862926645106,-4.55675964985629,331.222607877707));
#9386=CARTESIAN_POINT('Ctrl Pts',(165.85552837767,-4.65403804727018,331.346527621965));
#9387=CARTESIAN_POINT('Ctrl Pts',(165.848127511144,-4.7513506196083,331.470490900534));
#9388=CARTESIAN_POINT('Ctrl Pts',(165.840726644618,-4.84366661757521,331.598293351291));
#9389=CARTESIAN_POINT('Ctrl Pts',(165.833325778092,-4.9306862675299,331.729485744765));
#9390=CARTESIAN_POINT('Ctrl Pts',(165.825916784708,-5.01780147337922,331.86082220003));
#9391=CARTESIAN_POINT('Ctrl Pts',(165.818507791323,-5.09960851014299,331.995555720806));
#9392=CARTESIAN_POINT('Ctrl Pts',(165.811098797938,-5.1758522060904,332.13321006992));
#9393=CARTESIAN_POINT('Ctrl Pts',(165.803685240358,-5.25214287078408,332.27094921886));
#9394=CARTESIAN_POINT('Ctrl Pts',(165.796271682778,-5.32286319824254,332.41161244888));
#9395=CARTESIAN_POINT('Ctrl Pts',(165.788858125198,-5.38780558673392,332.554702160869));
#9396=CARTESIAN_POINT('Ctrl Pts',(165.781434013061,-5.45284043260494,332.69799558726));
#9397=CARTESIAN_POINT('Ctrl Pts',(165.774009900924,-5.51208077046498,332.843722050228));
#9398=CARTESIAN_POINT('Ctrl Pts',(165.766585788787,-5.5653681287757,332.991366595491));
#9399=CARTESIAN_POINT('Ctrl Pts',(165.762728663633,-5.59305305680225,333.068073881022));
#9400=CARTESIAN_POINT('Ctrl Pts',(165.758871538478,-5.61913197552565,333.145298682617));
#9401=CARTESIAN_POINT('Ctrl Pts',(165.755014413324,-5.64358809952865,333.22296766339));
#9402=CARTESIAN_POINT('Ctrl Pts',(165.746023029526,-5.70059801969011,333.404022616836));
#9403=CARTESIAN_POINT('Ctrl Pts',(165.737031645728,-5.74892617985712,333.587933734667));
#9404=CARTESIAN_POINT('Ctrl Pts',(165.72804026193,-5.78832629189741,333.773945637001));
#9405=CARTESIAN_POINT('Ctrl Pts',(165.719102717181,-5.8274904820159,333.95884372815));
#9406=CARTESIAN_POINT('Ctrl Pts',(165.710165172431,-5.85783316547064,334.145817522432));
#9407=CARTESIAN_POINT('Ctrl Pts',(165.701227627682,-5.87915919723639,334.334103839889));
#9408=CARTESIAN_POINT('Ctrl Pts',(165.692387285589,-5.90025329204519,334.520342399189));
#9409=CARTESIAN_POINT('Ctrl Pts',(165.683546943495,-5.91252573367141,334.707865066868));
#9410=CARTESIAN_POINT('Ctrl Pts',(165.674706601402,-5.91583437631538,334.895912563173));
#9411=CARTESIAN_POINT('Ctrl Pts',(165.67315508713,-5.91641505591232,334.928915627));
#9412=CARTESIAN_POINT('Ctrl Pts',(165.671603572858,-5.9167197549969,334.961934804774));
#9413=CARTESIAN_POINT('Ctrl Pts',(165.670052058585,-5.91674785846066,334.994965925983));
#9414=CARTESIAN_POINT('',(163.92005197593,-5.91236359159777,335.002943397715));
#9415=CARTESIAN_POINT('Ctrl Pts',(165.670052004703,-5.9125949101779,334.994970605717));
#9416=CARTESIAN_POINT('Ctrl Pts',(165.605626796152,-5.90157047433765,336.365605316277));
#9417=CARTESIAN_POINT('Ctrl Pts',(165.448455576177,-4.74432772518099,339.726187368728));
#9418=CARTESIAN_POINT('Ctrl Pts',(165.198538344775,0.852320882572409,341.944506608418));
#9419=CARTESIAN_POINT('Ctrl Pts',(164.920300310502,6.30102349729095,338.041336187897));
#9420=CARTESIAN_POINT('Ctrl Pts',(164.642062276227,5.96736985149999,331.347176437792));
#9421=CARTESIAN_POINT('Ctrl Pts',(164.363824241953,0.157548971222278,328.005158955138));
#9422=CARTESIAN_POINT('Ctrl Pts',(164.123154151445,-4.99288378853887,330.666738550612));
#9423=CARTESIAN_POINT('Ctrl Pts',(163.975230072362,-5.90312434765324,333.826940535229));
#9424=CARTESIAN_POINT('Ctrl Pts',(163.920052004703,-5.90839865240753,335.00294081012));
#9425=CARTESIAN_POINT('',(162.170052004703,-5.92027431987653,335.003792543636));
#9426=CARTESIAN_POINT('Ctrl Pts',(163.920051944103,-5.91674926645136,335.002946259889));
#9427=CARTESIAN_POINT('Ctrl Pts',(163.911914879253,-5.91666278780247,335.17661474182));
#9428=CARTESIAN_POINT('Ctrl Pts',(163.903777814403,-5.90892594379626,335.350022803605));
#9429=CARTESIAN_POINT('Ctrl Pts',(163.895640749552,-5.8936319271713,335.522525855367));
#9430=CARTESIAN_POINT('Ctrl Pts',(163.887462804686,-5.87826107453063,335.695895549786));
#9431=CARTESIAN_POINT('Ctrl Pts',(163.87928485982,-5.85525700650048,335.868350886963));
#9432=CARTESIAN_POINT('Ctrl Pts',(163.871106914954,-5.82476469640279,336.03925299809));
#9433=CARTESIAN_POINT('Ctrl Pts',(163.862908238715,-5.79419508724312,336.210588351987));
#9434=CARTESIAN_POINT('Ctrl Pts',(163.854709562475,-5.75609933448853,336.380362378213));
#9435=CARTESIAN_POINT('Ctrl Pts',(163.846510886235,-5.71067252318331,336.547950223831));
#9436=CARTESIAN_POINT('Ctrl Pts',(163.838282869471,-5.66508314337878,336.716137814485));
#9437=CARTESIAN_POINT('Ctrl Pts',(163.830054852706,-5.61211025401772,336.882123336397));
#9438=CARTESIAN_POINT('Ctrl Pts',(163.821826835942,-5.55199864370271,337.045297441162));
#9439=CARTESIAN_POINT('Ctrl Pts',(163.817000615097,-5.5167396116611,337.141008751475));
#9440=CARTESIAN_POINT('Ctrl Pts',(163.812174394251,-5.47902537499804,337.235753222751));
#9441=CARTESIAN_POINT('Ctrl Pts',(163.807348173406,-5.43891266166284,337.329411861673));
#9442=CARTESIAN_POINT('Ctrl Pts',(163.799924195968,-5.37720892113168,337.473483101787));
#9443=CARTESIAN_POINT('Ctrl Pts',(163.79250021853,-5.30968369431148,337.615318283778));
#9444=CARTESIAN_POINT('Ctrl Pts',(163.785076241092,-5.23652009251177,337.754412438837));
#9445=CARTESIAN_POINT('Ctrl Pts',(163.777661025064,-5.16344283477019,337.893342441866));
#9446=CARTESIAN_POINT('Ctrl Pts',(163.770245809037,-5.08474061925313,338.029537529839));
#9447=CARTESIAN_POINT('Ctrl Pts',(163.762830593009,-5.00064491737444,338.162511813865));
#9448=CARTESIAN_POINT('Ctrl Pts',(163.755422511865,-4.91663013195663,338.295358150705));
#9449=CARTESIAN_POINT('Ctrl Pts',(163.748014430721,-4.82723238982313,338.424989539893));
#9450=CARTESIAN_POINT('Ctrl Pts',(163.740606349577,-4.73272939838828,338.550943959588));
#9451=CARTESIAN_POINT('Ctrl Pts',(163.733203782403,-4.63829674725599,338.676804629107));
#9452=CARTESIAN_POINT('Ctrl Pts',(163.725801215229,-4.53876663606076,338.798993481325));
#9453=CARTESIAN_POINT('Ctrl Pts',(163.718398648055,-4.43446040394281,338.917076906108));
#9454=CARTESIAN_POINT('Ctrl Pts',(163.7109999783,-4.33020908860024,339.035098160484));
#9455=CARTESIAN_POINT('Ctrl Pts',(163.703601308545,-4.22118690677906,339.149018013152));
#9456=CARTESIAN_POINT('Ctrl Pts',(163.69620263879,-4.10775577263092,339.258435519638));
#9457=CARTESIAN_POINT('Ctrl Pts',(163.688805189586,-3.99434335109758,339.367834975634));
#9458=CARTESIAN_POINT('Ctrl Pts',(163.681407740382,-3.87652368912112,339.472733300709));
#9459=CARTESIAN_POINT('Ctrl Pts',(163.674010291178,-3.75469597389218,339.572765979813));
#9460=CARTESIAN_POINT('Ctrl Pts',(163.666613162715,-3.63287354090064,339.672794321675));
#9461=CARTESIAN_POINT('Ctrl Pts',(163.659216034251,-3.50704368862962,339.767957200201));
#9462=CARTESIAN_POINT('Ctrl Pts',(163.651818905788,-3.377638924035,339.857930203424));
#9463=CARTESIAN_POINT('Ctrl Pts',(163.644420638351,-3.24821423433705,339.947917060244));
#9464=CARTESIAN_POINT('Ctrl Pts',(163.637022370915,-3.11521384274522,340.03271223756));
#9465=CARTESIAN_POINT('Ctrl Pts',(163.629624103478,-2.97909935202512,340.11203458647));
#9466=CARTESIAN_POINT('Ctrl Pts',(163.622223236952,-2.84293704285288,340.191384802155));
#9467=CARTESIAN_POINT('Ctrl Pts',(163.614822370427,-2.70365877861787,340.265258173621));
#9468=CARTESIAN_POINT('Ctrl Pts',(163.607421503901,-2.56175072887888,340.333419518994));
#9469=CARTESIAN_POINT('Ctrl Pts',(163.600012510516,-2.41968685053427,340.401655712041));
#9470=CARTESIAN_POINT('Ctrl Pts',(163.592603517131,-2.27498775630009,340.46416719109));
#9471=CARTESIAN_POINT('Ctrl Pts',(163.585194523746,-2.12816023657423,340.520766665053));
#9472=CARTESIAN_POINT('Ctrl Pts',(163.577780966166,-1.98124226603168,340.577401006245));
#9473=CARTESIAN_POINT('Ctrl Pts',(163.570367408586,-1.83219360978396,340.628115965247));
#9474=CARTESIAN_POINT('Ctrl Pts',(163.562953851006,-1.68153567892164,340.672774305665));
#9475=CARTESIAN_POINT('Ctrl Pts',(163.555529738869,-1.53066325891303,340.717496225407));
#9476=CARTESIAN_POINT('Ctrl Pts',(163.548105626732,-1.37817734930732,340.756144213852));
#9477=CARTESIAN_POINT('Ctrl Pts',(163.540681514596,-1.22460979870516,340.788632083957));
#9478=CARTESIAN_POINT('Ctrl Pts',(163.536824389441,-1.14482527344265,340.805510840458));
#9479=CARTESIAN_POINT('Ctrl Pts',(163.532967264287,-1.06474888976958,340.820727698219));
#9480=CARTESIAN_POINT('Ctrl Pts',(163.529110139132,-0.984455595665917,340.834276111281));
#9481=CARTESIAN_POINT('Ctrl Pts',(163.521686161694,-0.829911581668405,340.860353334308));
#9482=CARTESIAN_POINT('Ctrl Pts',(163.514262184256,-0.674097576382707,340.880325085964));
#9483=CARTESIAN_POINT('Ctrl Pts',(163.506838206818,-0.517537310889843,340.894072080857));
#9484=CARTESIAN_POINT('Ctrl Pts',(163.499422990791,-0.361161810065995,340.907802852228));
#9485=CARTESIAN_POINT('Ctrl Pts',(163.492007774763,-0.204042170246386,340.915323457136));
#9486=CARTESIAN_POINT('Ctrl Pts',(163.484592558736,-0.0467122482306003,
340.916565602473));
#9487=CARTESIAN_POINT('Ctrl Pts',(163.477184477591,0.110466291726413,340.917806552623));
#9488=CARTESIAN_POINT('Ctrl Pts',(163.469776396447,0.267854340367967,340.912781066983));
#9489=CARTESIAN_POINT('Ctrl Pts',(163.462368315303,0.424913090254497,340.901472649113));
#9490=CARTESIAN_POINT('Ctrl Pts',(163.454965748129,0.581854938444996,340.890172648305));
#9491=CARTESIAN_POINT('Ctrl Pts',(163.447563180955,0.738467605263232,340.872599053549));
#9492=CARTESIAN_POINT('Ctrl Pts',(163.440160613781,0.894212563651498,340.848787434461));
#9493=CARTESIAN_POINT('Ctrl Pts',(163.432761944026,1.04987552300004,340.824988352086));
#9494=CARTESIAN_POINT('Ctrl Pts',(163.425363274272,1.20467131575669,340.794957842505));
#9495=CARTESIAN_POINT('Ctrl Pts',(163.417964604517,1.35806692664593,340.758783272988));
#9496=CARTESIAN_POINT('Ctrl Pts',(163.410567155313,1.51143723202248,340.722614671152));
#9497=CARTESIAN_POINT('Ctrl Pts',(163.403169706109,1.66340745107125,340.680304106587));
#9498=CARTESIAN_POINT('Ctrl Pts',(163.395772256905,1.81345503221666,340.631990004308));
#9499=CARTESIAN_POINT('Ctrl Pts',(163.388375128442,1.96349610756049,340.583677996845));
#9500=CARTESIAN_POINT('Ctrl Pts',(163.380977999978,2.11161435550307,340.529363083624));
#9501=CARTESIAN_POINT('Ctrl Pts',(163.373580871515,2.25730291676891,340.469233411041));
#9502=CARTESIAN_POINT('Ctrl Pts',(163.366182604078,2.40301391043637,340.40909447999));
#9503=CARTESIAN_POINT('Ctrl Pts',(163.358784336641,2.54629412751842,340.343139149254));
#9504=CARTESIAN_POINT('Ctrl Pts',(163.351386069205,2.68665734416086,340.271603444642));
#9505=CARTESIAN_POINT('Ctrl Pts',(163.343985202679,2.82706987187757,340.200042608786));
#9506=CARTESIAN_POINT('Ctrl Pts',(163.336584336153,2.96456302652566,340.122897665174));
#9507=CARTESIAN_POINT('Ctrl Pts',(163.329183469627,3.09867594440411,340.040450173751));
#9508=CARTESIAN_POINT('Ctrl Pts',(163.321774476243,3.23293613108799,339.957912147102));
#9509=CARTESIAN_POINT('Ctrl Pts',(163.314365482858,3.36380835016669,339.870060139962));
#9510=CARTESIAN_POINT('Ctrl Pts',(163.306956489473,3.49086085120392,339.777218969236));
#9511=CARTESIAN_POINT('Ctrl Pts',(163.299542931893,3.61799162096432,339.684320605147));
#9512=CARTESIAN_POINT('Ctrl Pts',(163.292129374313,3.74129769225111,339.586427184635));
#9513=CARTESIAN_POINT('Ctrl Pts',(163.284715816732,3.86038149459243,339.483902906923));
#9514=CARTESIAN_POINT('Ctrl Pts',(163.277291704596,3.9796348345275,339.381232667131));
#9515=CARTESIAN_POINT('Ctrl Pts',(163.269867592459,4.09465362785683,339.273918656769));
#9516=CARTESIAN_POINT('Ctrl Pts',(163.262443480322,4.20507758426156,339.162361477916));
#9517=CARTESIAN_POINT('Ctrl Pts',(163.258586355168,4.26244727535505,339.104403032137));
#9518=CARTESIAN_POINT('Ctrl Pts',(163.254729230013,4.31857738167461,339.045299807624));
#9519=CARTESIAN_POINT('Ctrl Pts',(163.250872104858,4.37342183993305,338.985111287342));
#9520=CARTESIAN_POINT('Ctrl Pts',(163.24344812742,4.47898336681745,338.86926381061));
#9521=CARTESIAN_POINT('Ctrl Pts',(163.236024149982,4.5800979377291,338.749044350219));
#9522=CARTESIAN_POINT('Ctrl Pts',(163.228600172544,4.67638182209828,338.624828770639));
#9523=CARTESIAN_POINT('Ctrl Pts',(163.221184956517,4.77255207699727,338.500759784131));
#9524=CARTESIAN_POINT('Ctrl Pts',(163.213769740489,4.8639027667394,338.372704357855));
#9525=CARTESIAN_POINT('Ctrl Pts',(163.206354524461,4.95008756164463,338.241074466061));
#9526=CARTESIAN_POINT('Ctrl Pts',(163.198946443317,5.03618942997412,338.109571227886));
#9527=CARTESIAN_POINT('Ctrl Pts',(163.191538362173,5.11713509592958,337.974500681415));
#9528=CARTESIAN_POINT('Ctrl Pts',(163.184130281029,5.19261910768074,337.836306994147));
#9529=CARTESIAN_POINT('Ctrl Pts',(163.176727713855,5.26804693530333,337.698216166965));
#9530=CARTESIAN_POINT('Ctrl Pts',(163.169325146681,5.3380210250051,337.557007153758));
#9531=CARTESIAN_POINT('Ctrl Pts',(163.161922579507,5.40227986014308,337.413152062178));
#9532=CARTESIAN_POINT('Ctrl Pts',(163.154523909752,5.46650486328523,337.269372709674));
#9533=CARTESIAN_POINT('Ctrl Pts',(163.147125239998,5.52502045274703,337.122950393237));
#9534=CARTESIAN_POINT('Ctrl Pts',(163.139726570243,5.57761165238015,336.974380616227));
#9535=CARTESIAN_POINT('Ctrl Pts',(163.132329121039,5.63019417609838,336.825835348617));
#9536=CARTESIAN_POINT('Ctrl Pts',(163.124931671835,5.67685412527571,336.67514367501));
#9537=CARTESIAN_POINT('Ctrl Pts',(163.117534222631,5.7174251218197,336.522819929895));
#9538=CARTESIAN_POINT('Ctrl Pts',(163.110137094167,5.757994359276,336.370502789272));
#9539=CARTESIAN_POINT('Ctrl Pts',(163.102739965704,5.79247507297557,336.21655407848));
#9540=CARTESIAN_POINT('Ctrl Pts',(163.095342837241,5.82075118859921,336.061501843108));
#9541=CARTESIAN_POINT('Ctrl Pts',(163.087944569804,5.8490316580388,335.906425733562));
#9542=CARTESIAN_POINT('Ctrl Pts',(163.080546302367,5.87110556020794,335.750246128291));
#9543=CARTESIAN_POINT('Ctrl Pts',(163.073148034931,5.88690825061817,335.593499630416));
#9544=CARTESIAN_POINT('Ctrl Pts',(163.065747168405,5.90271649267974,335.436698065847));
#9545=CARTESIAN_POINT('Ctrl Pts',(163.058346301879,5.91224909911652,335.279329583252));
#9546=CARTESIAN_POINT('Ctrl Pts',(163.050945435354,5.91549343990135,335.12193410099));
#9547=CARTESIAN_POINT('Ctrl Pts',(163.043536441969,5.91874134328252,334.96436578344));
#9548=CARTESIAN_POINT('Ctrl Pts',(163.036127448584,5.91568718342874,334.806770780371));
#9549=CARTESIAN_POINT('Ctrl Pts',(163.028718455199,5.90637046086806,334.649687936997));
#9550=CARTESIAN_POINT('Ctrl Pts',(163.021304897619,5.89704799888492,334.492508325174));
#9551=CARTESIAN_POINT('Ctrl Pts',(163.013891340039,5.88145532358617,334.335841872247));
#9552=CARTESIAN_POINT('Ctrl Pts',(163.006477782459,5.85968354967255,334.180219992805));
#9553=CARTESIAN_POINT('Ctrl Pts',(162.999053670322,5.83788077965292,334.024376557127));
#9554=CARTESIAN_POINT('Ctrl Pts',(162.991629558185,5.80988140774299,333.869581031314));
#9555=CARTESIAN_POINT('Ctrl Pts',(162.984205446049,5.77582733501344,333.716353179955));
#9556=CARTESIAN_POINT('Ctrl Pts',(162.980348320894,5.75813487319067,333.636745142118));
#9557=CARTESIAN_POINT('Ctrl Pts',(162.976491195739,5.73880893206018,333.557559992103));
#9558=CARTESIAN_POINT('Ctrl Pts',(162.972634070584,5.71787460462632,333.478868655155));
#9559=CARTESIAN_POINT('Ctrl Pts',(162.965210093146,5.67758138926146,333.327407998155));
#9560=CARTESIAN_POINT('Ctrl Pts',(162.957786115708,5.63120517652213,333.177320950082));
#9561=CARTESIAN_POINT('Ctrl Pts',(162.95036213827,5.57885438022989,333.02913359999));
#9562=CARTESIAN_POINT('Ctrl Pts',(162.942946922243,5.52656536575387,332.881121133266));
#9563=CARTESIAN_POINT('Ctrl Pts',(162.935531706215,5.46831592577613,332.735004250404));
#9564=CARTESIAN_POINT('Ctrl Pts',(162.928116490187,5.40426507937176,332.591297130325));
#9565=CARTESIAN_POINT('Ctrl Pts',(162.920708409043,5.34027586236931,332.447728284513));
#9566=CARTESIAN_POINT('Ctrl Pts',(162.913300327899,5.27049650274748,332.306564924069));
#9567=CARTESIAN_POINT('Ctrl Pts',(162.905892246755,5.19513521292146,332.168304274474));
#9568=CARTESIAN_POINT('Ctrl Pts',(162.898489679581,5.1198300158798,332.030146534805));
#9569=CARTESIAN_POINT('Ctrl Pts',(162.891087112407,5.03895133916165,331.894887530325));
#9570=CARTESIAN_POINT('Ctrl Pts',(162.883684545233,4.95275466650203,331.763002660498));
#9571=CARTESIAN_POINT('Ctrl Pts',(162.876285875478,4.86660337601388,331.631187227478));
#9572=CARTESIAN_POINT('Ctrl Pts',(162.868887205724,4.77513986942057,331.50274270279));
#9573=CARTESIAN_POINT('Ctrl Pts',(162.861488535969,4.67866449013922,331.378118009762));
#9574=CARTESIAN_POINT('Ctrl Pts',(162.854091086765,4.58220502629965,331.253513875939));
#9575=CARTESIAN_POINT('Ctrl Pts',(162.846693637561,4.48073555894519,331.132728617954));
#9576=CARTESIAN_POINT('Ctrl Pts',(162.839296188357,4.37459856618621,331.016180482599));
#9577=CARTESIAN_POINT('Ctrl Pts',(162.831899059893,4.26846617534221,330.899637400569));
#9578=CARTESIAN_POINT('Ctrl Pts',(162.82450193143,4.15766691277109,330.78733135182));
#9579=CARTESIAN_POINT('Ctrl Pts',(162.817104802967,4.04258200879939,330.679645701493));
#9580=CARTESIAN_POINT('Ctrl Pts',(162.80970653553,3.92747938462536,330.571943470263));
#9581=CARTESIAN_POINT('Ctrl Pts',(162.802308268093,3.80809007767113,330.468863309007));
#9582=CARTESIAN_POINT('Ctrl Pts',(162.794910000657,3.68483034610691,330.370749965393));
#9583=CARTESIAN_POINT('Ctrl Pts',(162.787509134131,3.56152731210267,330.272602153529));
#9584=CARTESIAN_POINT('Ctrl Pts',(162.780108267605,3.43435143810209,330.179424865673));
#9585=CARTESIAN_POINT('Ctrl Pts',(162.772707401079,3.30374991814138,330.091520903489));
#9586=CARTESIAN_POINT('Ctrl Pts',(162.765298407695,3.17300498522576,330.003520414351));
#9587=CARTESIAN_POINT('Ctrl Pts',(162.75788941431,3.03882720385781,329.92080502357));
#9588=CARTESIAN_POINT('Ctrl Pts',(162.750480420925,2.90169107647838,329.843633114373));
#9589=CARTESIAN_POINT('Ctrl Pts',(162.743066863345,2.7644704685141,329.766413664619));
#9590=CARTESIAN_POINT('Ctrl Pts',(162.735653305765,2.62428821460374,329.694744670735));
#9591=CARTESIAN_POINT('Ctrl Pts',(162.728239748184,2.48164050000462,329.628837091352));
#9592=CARTESIAN_POINT('Ctrl Pts',(162.720815636048,2.33878970026872,329.562835680463));
#9593=CARTESIAN_POINT('Ctrl Pts',(162.713391523911,2.19346677345098,329.50261220846));
#9594=CARTESIAN_POINT('Ctrl Pts',(162.705967411774,2.04618559149351,329.448328622148));
#9595=CARTESIAN_POINT('Ctrl Pts',(162.70211028662,1.96966708782925,329.420126113565));
#9596=CARTESIAN_POINT('Ctrl Pts',(162.698253161465,1.89262023017412,329.393526081447));
#9597=CARTESIAN_POINT('Ctrl Pts',(162.69439603631,1.81511824034429,329.368545806271));
#9598=CARTESIAN_POINT('Ctrl Pts',(162.686972058872,1.66594677174351,329.320465178376));
#9599=CARTESIAN_POINT('Ctrl Pts',(162.679548081434,1.5146385412722,329.278243211356));
#9600=CARTESIAN_POINT('Ctrl Pts',(162.672124103996,1.36169461737936,329.24207343469));
#9601=CARTESIAN_POINT('Ctrl Pts',(162.664708887969,1.20893119032833,329.205946343803));
#9602=CARTESIAN_POINT('Ctrl Pts',(162.657293671941,1.05453627193794,329.175857311075));
#9603=CARTESIAN_POINT('Ctrl Pts',(162.649878455913,0.899028300580285,329.151950865694));
#9604=CARTESIAN_POINT('Ctrl Pts',(162.642470374769,0.743669958209789,329.128067422974));
#9605=CARTESIAN_POINT('Ctrl Pts',(162.635062293625,0.587201061394004,329.110354780869));
#9606=CARTESIAN_POINT('Ctrl Pts',(162.627654212481,0.430152413333387,329.098906926357));
#9607=CARTESIAN_POINT('Ctrl Pts',(162.620251645307,0.273220659449661,329.087467592691));
#9608=CARTESIAN_POINT('Ctrl Pts',(162.612849078133,0.115710384168476,329.08228378893));
#9609=CARTESIAN_POINT('Ctrl Pts',(162.605446510959,-0.0418403820498371,
329.083397939279));
#9610=CARTESIAN_POINT('Ctrl Pts',(162.598047841204,-0.199308198478223,329.084511503033));
#9611=CARTESIAN_POINT('Ctrl Pts',(162.59064917145,-0.356816091125044,329.091916414561));
#9612=CARTESIAN_POINT('Ctrl Pts',(162.583250501695,-0.513824017728563,329.10560304685));
#9613=CARTESIAN_POINT('Ctrl Pts',(162.575853052491,-0.670806042899634,329.119287421269));
#9614=CARTESIAN_POINT('Ctrl Pts',(162.568455603287,-0.827287894281514,329.139251427372));
#9615=CARTESIAN_POINT('Ctrl Pts',(162.561058154083,-0.982732524667903,329.165433405345));
#9616=CARTESIAN_POINT('Ctrl Pts',(162.55366102562,-1.13817041524606,329.191614248114));
#9617=CARTESIAN_POINT('Ctrl Pts',(162.546263897156,-1.29257080622066,329.224012464711));
#9618=CARTESIAN_POINT('Ctrl Pts',(162.538866768693,-1.44540501206314,329.262514931296));
#9619=CARTESIAN_POINT('Ctrl Pts',(162.531468501256,-1.598262750558,329.3010233263));
#9620=CARTESIAN_POINT('Ctrl Pts',(162.524070233819,-1.74955346182676,329.345637751582));
#9621=CARTESIAN_POINT('Ctrl Pts',(162.516671966383,-1.89876197901937,329.396194729514));
#9622=CARTESIAN_POINT('Ctrl Pts',(162.509271099857,-2.04802291473358,329.446769468643));
#9623=CARTESIAN_POINT('Ctrl Pts',(162.501870233331,-2.19519984671405,329.503290797298));
#9624=CARTESIAN_POINT('Ctrl Pts',(162.494469366805,-2.33979614022765,329.565546523828));
#9625=CARTESIAN_POINT('Ctrl Pts',(162.487060373421,-2.4845512142954,329.627870613098));
#9626=CARTESIAN_POINT('Ctrl Pts',(162.479651380036,-2.62671964767688,329.695941527848));
#9627=CARTESIAN_POINT('Ctrl Pts',(162.472242386651,-2.76582737990481,329.769500074843));
#9628=CARTESIAN_POINT('Ctrl Pts',(162.464828829071,-2.90502080729398,329.84310393644));
#9629=CARTESIAN_POINT('Ctrl Pts',(162.457415271491,-3.0411494544888,329.922201979454));
#9630=CARTESIAN_POINT('Ctrl Pts',(162.45000171391,-3.17376740756234,330.006491112935));
#9631=CARTESIAN_POINT('Ctrl Pts',(162.442577601774,-3.30657416657106,330.090900247429));
#9632=CARTESIAN_POINT('Ctrl Pts',(162.435153489637,-3.43585994331866,330.180515020596));
#9633=CARTESIAN_POINT('Ctrl Pts',(162.4277293775,-3.56121046768816,330.274990945265));
#9634=CARTESIAN_POINT('Ctrl Pts',(162.423872252346,-3.62633511179299,330.324074991794));
#9635=CARTESIAN_POINT('Ctrl Pts',(162.420015127191,-3.69039812191298,330.37447053443));
#9636=CARTESIAN_POINT('Ctrl Pts',(162.416158002036,-3.75334534200005,330.426125350845));
#9637=CARTESIAN_POINT('Ctrl Pts',(162.408834076206,-3.87286979418515,330.524207738377));
#9638=CARTESIAN_POINT('Ctrl Pts',(162.401510150377,-3.98875087258847,330.62714595177));
#9639=CARTESIAN_POINT('Ctrl Pts',(162.394186224547,-4.10056070490289,330.734635716858));
#9640=CARTESIAN_POINT('Ctrl Pts',(162.386870990571,-4.21223784407263,330.84199791575));
#9641=CARTESIAN_POINT('Ctrl Pts',(162.379555756595,-4.31985307605865,330.953900655882));
#9642=CARTESIAN_POINT('Ctrl Pts',(162.372240522619,-4.42300982275395,331.069998133547));
#9643=CARTESIAN_POINT('Ctrl Pts',(162.364932271489,-4.52606809992302,331.185984788955));
#9644=CARTESIAN_POINT('Ctrl Pts',(162.357624020358,-4.62467610732625,331.306157928751));
#9645=CARTESIAN_POINT('Ctrl Pts',(162.350315769228,-4.71847271683409,331.43013364634));
#9646=CARTESIAN_POINT('Ctrl Pts',(162.342804779039,-4.81487134916897,331.55754858896));
#9647=CARTESIAN_POINT('Ctrl Pts',(162.335293788851,-4.90618744902999,331.688979879911));
#9648=CARTESIAN_POINT('Ctrl Pts',(162.327782798662,-4.99207144355252,331.823972093169));
#9649=CARTESIAN_POINT('Ctrl Pts',(162.320483051653,-5.07553998983188,331.955167711892));
#9650=CARTESIAN_POINT('Ctrl Pts',(162.313183304644,-5.15387765041819,332.089726301311));
#9651=CARTESIAN_POINT('Ctrl Pts',(162.305883557635,-5.22680629540618,332.22719879674));
#9652=CARTESIAN_POINT('Ctrl Pts',(162.298585222039,-5.29972083956195,332.364644711712));
#9653=CARTESIAN_POINT('Ctrl Pts',(162.291286886444,-5.36722826889103,332.505003072579));
#9654=CARTESIAN_POINT('Ctrl Pts',(162.283988550849,-5.42909594822425,332.647799381967));
#9655=CARTESIAN_POINT('Ctrl Pts',(162.276690094723,-5.49096464928864,332.790598049604));
#9656=CARTESIAN_POINT('Ctrl Pts',(162.269391638598,-5.54719326293106,332.935834393082));
#9657=CARTESIAN_POINT('Ctrl Pts',(162.262093182472,-5.59759705042366,333.083013348093));
#9658=CARTESIAN_POINT('Ctrl Pts',(162.254423084325,-5.65056743079071,333.237686748979));
#9659=CARTESIAN_POINT('Ctrl Pts',(162.246752986177,-5.69710406747602,333.39450534185));
#9660=CARTESIAN_POINT('Ctrl Pts',(162.23908288803,-5.73705189812322,333.552876618688));
#9661=CARTESIAN_POINT('Ctrl Pts',(162.231776197098,-5.77510701115041,333.703744306437));
#9662=CARTESIAN_POINT('Ctrl Pts',(162.224469506166,-5.80718324959507,333.856020543179));
#9663=CARTESIAN_POINT('Ctrl Pts',(162.217162815235,-5.8331992311469,334.009183522418));
#9664=CARTESIAN_POINT('Ctrl Pts',(162.209852166545,-5.85922930457227,334.162429464252));
#9665=CARTESIAN_POINT('Ctrl Pts',(162.202541517855,-5.87919253479397,334.316562725204));
#9666=CARTESIAN_POINT('Ctrl Pts',(162.195230869165,-5.89305947556703,334.4710571109));
#9667=CARTESIAN_POINT('Ctrl Pts',(162.187911768722,-5.90694244774457,334.625730105708));
#9668=CARTESIAN_POINT('Ctrl Pts',(162.180592668278,-5.91471504814765,334.780764676496));
#9669=CARTESIAN_POINT('Ctrl Pts',(162.173273567835,-5.91639989463546,334.93563503082));
#9670=CARTESIAN_POINT('Ctrl Pts',(162.172199713458,-5.9166470943822,334.958357523725));
#9671=CARTESIAN_POINT('Ctrl Pts',(162.17112585908,-5.91676333648397,334.981076491471));
#9672=CARTESIAN_POINT('Ctrl Pts',(162.170052004703,-5.91674878596669,335.00379028517));
#9673=CARTESIAN_POINT('',(160.420052004703,-5.91893227834984,334.995030093563));
#9674=CARTESIAN_POINT('Ctrl Pts',(162.170052004703,-5.92337931611586,335.003794532705));
#9675=CARTESIAN_POINT('Ctrl Pts',(162.159341325723,-5.92507004615438,335.230598138262));
#9676=CARTESIAN_POINT('Ctrl Pts',(162.055884635312,-5.8101798197072,337.419612438354));
#9677=CARTESIAN_POINT('Ctrl Pts',(161.859681933494,-3.08383468430733,341.280333316078));
#9678=CARTESIAN_POINT('Ctrl Pts',(161.581443899212,3.61242637245241,340.991911099545));
#9679=CARTESIAN_POINT('Ctrl Pts',(161.303205864942,6.99361706653863,335.204800507416));
#9680=CARTESIAN_POINT('Ctrl Pts',(161.024967830666,3.95686860428096,329.229747512485));
#9681=CARTESIAN_POINT('Ctrl Pts',(160.746729796393,-2.71103977284048,328.549970056558));
#9682=CARTESIAN_POINT('Ctrl Pts',(160.545091187738,-5.74029804598019,332.346895813797));
#9683=CARTESIAN_POINT('Ctrl Pts',(160.436198590508,-5.92331568745704,334.65264523622));
#9684=CARTESIAN_POINT('Ctrl Pts',(160.420052004703,-5.92023889988851,334.995028996442));
#9685=CARTESIAN_POINT('',(158.670052029646,-5.9115263163086,334.998821163383));
#9686=CARTESIAN_POINT('Ctrl Pts',(160.420052004703,-5.91674791424796,334.995031927692));
#9687=CARTESIAN_POINT('Ctrl Pts',(160.412749604594,-5.91687785434,335.149784660933));
#9688=CARTESIAN_POINT('Ctrl Pts',(160.405447204486,-5.91093230913336,335.304751775812));
#9689=CARTESIAN_POINT('Ctrl Pts',(160.398144804377,-5.89888753872582,335.459408715596));
#9690=CARTESIAN_POINT('Ctrl Pts',(160.390848879078,-5.88685344803854,335.61392852592));
#9691=CARTESIAN_POINT('Ctrl Pts',(160.383552953779,-5.86873092290481,335.768138326656));
#9692=CARTESIAN_POINT('Ctrl Pts',(160.376257028479,-5.84454826906993,335.921512936975));
#9693=CARTESIAN_POINT('Ctrl Pts',(160.368965870975,-5.82038141829307,336.074787318928));
#9694=CARTESIAN_POINT('Ctrl Pts',(160.36167471347,-5.79016238049308,336.227227217478));
#9695=CARTESIAN_POINT('Ctrl Pts',(160.354383555966,-5.75397132106502,336.378312228365));
#9696=CARTESIAN_POINT('Ctrl Pts',(160.347094686519,-5.71779161884968,336.529349826863));
#9697=CARTESIAN_POINT('Ctrl Pts',(160.339805817072,-5.67564370952146,336.679033008618));
#9698=CARTESIAN_POINT('Ctrl Pts',(160.332516947625,-5.6276589060248,336.826851334931));
#9699=CARTESIAN_POINT('Ctrl Pts',(160.325229030337,-5.57968037087738,336.974650351445));
#9700=CARTESIAN_POINT('Ctrl Pts',(160.317941113049,-5.52586657691341,337.120584630543));
#9701=CARTESIAN_POINT('Ctrl Pts',(160.310653195762,-5.46639867417403,337.264159026546));
#9702=CARTESIAN_POINT('Ctrl Pts',(160.303364692781,-5.40692599230215,337.407744960892));
#9703=CARTESIAN_POINT('Ctrl Pts',(160.296076189801,-5.34179844518155,337.548970278778));
#9704=CARTESIAN_POINT('Ctrl Pts',(160.28878768682,-5.27124515581358,337.687360241912));
#9705=CARTESIAN_POINT('Ctrl Pts',(160.281497059991,-5.20067130742247,337.825790531479));
#9706=CARTESIAN_POINT('Ctrl Pts',(160.274206433162,-5.12466874639831,337.961383479486));
#9707=CARTESIAN_POINT('Ctrl Pts',(160.266915806333,-5.04351216682569,338.093689639505));
#9708=CARTESIAN_POINT('Ctrl Pts',(160.259617581489,-4.96227100894461,338.226133683985));
#9709=CARTESIAN_POINT('Ctrl Pts',(160.252319356645,-4.87586531029611,338.355283773128));
#9710=CARTESIAN_POINT('Ctrl Pts',(160.245021131802,-4.78461294959435,338.480719679186));
#9711=CARTESIAN_POINT('Ctrl Pts',(160.237718620924,-4.69330699905403,338.606229250078));
#9712=CARTESIAN_POINT('Ctrl Pts',(160.230416110047,-4.5971489570975,338.72801999315));
#9713=CARTESIAN_POINT('Ctrl Pts',(160.223113599169,-4.49649592147139,338.845706045799));
#9714=CARTESIAN_POINT('Ctrl Pts',(160.215800846283,-4.39570171668679,338.963557156966));
#9715=CARTESIAN_POINT('Ctrl Pts',(160.208488093396,-4.29040019302738,339.077291802976));
#9716=CARTESIAN_POINT('Ctrl Pts',(160.201175340509,-4.18098452699986,339.186561709504));
#9717=CARTESIAN_POINT('Ctrl Pts',(160.197534802954,-4.12651368032173,339.240959992137));
#9718=CARTESIAN_POINT('Ctrl Pts',(160.193894265399,-4.07102369912965,339.294252372113));
#9719=CARTESIAN_POINT('Ctrl Pts',(160.190253727844,-4.01456592510909,339.346399774003));
#9720=CARTESIAN_POINT('Ctrl Pts',(160.182829750406,-3.89943423529873,339.452741524152));
#9721=CARTESIAN_POINT('Ctrl Pts',(160.175405772968,-3.77990061924428,339.55466595567));
#9722=CARTESIAN_POINT('Ctrl Pts',(160.16798179553,-3.656338340465,339.651786807512));
#9723=CARTESIAN_POINT('Ctrl Pts',(160.160566579503,-3.5329218837653,339.748793042137));
#9724=CARTESIAN_POINT('Ctrl Pts',(160.153151363475,-3.40548651867336,339.841006752827));
#9725=CARTESIAN_POINT('Ctrl Pts',(160.145736147447,-3.274441870336,339.928078834626));
#9726=CARTESIAN_POINT('Ctrl Pts',(160.138328066303,-3.14352331249969,340.015067136106));
#9727=CARTESIAN_POINT('Ctrl Pts',(160.130919985159,-3.00900269395467,340.096923452584));
#9728=CARTESIAN_POINT('Ctrl Pts',(160.123511904015,-2.87132210852129,340.173339338533));
#9729=CARTESIAN_POINT('Ctrl Pts',(160.116109336841,-2.73374400126222,340.249698346743));
#9730=CARTESIAN_POINT('Ctrl Pts',(160.108706769667,-2.59301093525265,340.320624807053));
#9731=CARTESIAN_POINT('Ctrl Pts',(160.101304202493,-2.44959324063972,340.385854019365));
#9732=CARTESIAN_POINT('Ctrl Pts',(160.093905532738,-2.30625105481628,340.451048888782));
#9733=CARTESIAN_POINT('Ctrl Pts',(160.086506862983,-2.16022739421783,340.510552329911));
#9734=CARTESIAN_POINT('Ctrl Pts',(160.079108193229,-2.01201629857973,340.564146024032));
#9735=CARTESIAN_POINT('Ctrl Pts',(160.071710744025,-1.86382965316995,340.617730876857));
#9736=CARTESIAN_POINT('Ctrl Pts',(160.064313294821,-1.71345663953757,340.665407790796));
#9737=CARTESIAN_POINT('Ctrl Pts',(160.056915845617,-1.56141045642998,340.707006916857));
#9738=CARTESIAN_POINT('Ctrl Pts',(160.049518717153,-1.40937086577999,340.748604239252));
#9739=CARTESIAN_POINT('Ctrl Pts',(160.04212158869,-1.25565860988089,340.784124199249));
#9740=CARTESIAN_POINT('Ctrl Pts',(160.034724460226,-1.1008009381068,340.813447157854));
#9741=CARTESIAN_POINT('Ctrl Pts',(160.02732619279,-0.945919422116997,340.842774631463));
#9742=CARTESIAN_POINT('Ctrl Pts',(160.019927925353,-0.789892505802936,340.865903134335));
#9743=CARTESIAN_POINT('Ctrl Pts',(160.012529657917,-0.63325634332054,340.88276439832));
#9744=CARTESIAN_POINT('Ctrl Pts',(160.005128791391,-0.476565152907182,340.899631585845));
#9745=CARTESIAN_POINT('Ctrl Pts',(159.997727924865,-0.319264661016791,340.910227110891));
#9746=CARTESIAN_POINT('Ctrl Pts',(159.990327058339,-0.161894688364802,340.914534696185));
#9747=CARTESIAN_POINT('Ctrl Pts',(159.982918064955,-0.00435190843748323,
340.91884701162));
#9748=CARTESIAN_POINT('Ctrl Pts',(159.97550907157,0.153260131325582,340.916857587913));
#9749=CARTESIAN_POINT('Ctrl Pts',(159.968100078185,0.310402331149898,340.908602284408));
#9750=CARTESIAN_POINT('Ctrl Pts',(159.960686520605,0.467641335989746,340.900341895352));
#9751=CARTESIAN_POINT('Ctrl Pts',(159.953272963025,0.624409553398733,340.885807969313));
#9752=CARTESIAN_POINT('Ctrl Pts',(159.945859405444,0.780174965370762,340.865088028829));
#9753=CARTESIAN_POINT('Ctrl Pts',(159.938435293308,0.936162137923267,340.844338589716));
#9754=CARTESIAN_POINT('Ctrl Pts',(159.931011181171,1.09114328698146,340.817385610743));
#9755=CARTESIAN_POINT('Ctrl Pts',(159.923587069034,1.24459770117596,340.784367478362));
#9756=CARTESIAN_POINT('Ctrl Pts',(159.91972994388,1.32432344752623,340.767213229258));
#9757=CARTESIAN_POINT('Ctrl Pts',(159.915872818725,1.40363735102046,340.748422681214));
#9758=CARTESIAN_POINT('Ctrl Pts',(159.91201569357,1.48246831851101,340.728020447512));
#9759=CARTESIAN_POINT('Ctrl Pts',(159.904591716132,1.63419772852416,340.688751376217));
#9760=CARTESIAN_POINT('Ctrl Pts',(159.897167738694,1.78459465593474,340.643390166656));
#9761=CARTESIAN_POINT('Ctrl Pts',(159.889743761256,1.93313229128134,340.59204167607));
#9762=CARTESIAN_POINT('Ctrl Pts',(159.882328545229,2.08149462986962,340.540753784429));
#9763=CARTESIAN_POINT('Ctrl Pts',(159.874913329201,2.22800169477283,340.483492797285));
#9764=CARTESIAN_POINT('Ctrl Pts',(159.867498113173,2.37213824451428,340.42041425644));
#9765=CARTESIAN_POINT('Ctrl Pts',(159.860090032029,2.5161361067931,340.357396409449));
#9766=CARTESIAN_POINT('Ctrl Pts',(159.852681950885,2.6577676551336,340.288572301203));
#9767=CARTESIAN_POINT('Ctrl Pts',(159.845273869741,2.79653426877775,340.214146780256));
#9768=CARTESIAN_POINT('Ctrl Pts',(159.837871302567,2.93519759589714,340.139776655583));
#9769=CARTESIAN_POINT('Ctrl Pts',(159.830468735393,3.070999906801,340.0598135954));
#9770=CARTESIAN_POINT('Ctrl Pts',(159.823066168219,3.20346408689925,339.974509865951));
#9771=CARTESIAN_POINT('Ctrl Pts',(159.815667498464,3.33585852518593,339.889251048543));
#9772=CARTESIAN_POINT('Ctrl Pts',(159.80826882871,3.46491801986771,339.798657363369));
#9773=CARTESIAN_POINT('Ctrl Pts',(159.800870158955,3.59019162882605,339.703026114196));
#9774=CARTESIAN_POINT('Ctrl Pts',(159.793472709751,3.71544457152872,339.607410641209));
#9775=CARTESIAN_POINT('Ctrl Pts',(159.786075260547,3.83691257168035,339.506759479811));
#9776=CARTESIAN_POINT('Ctrl Pts',(159.778677811343,3.954175078351,339.401412274742));
#9777=CARTESIAN_POINT('Ctrl Pts',(159.771280682879,4.07143250072357,339.296069637344));
#9778=CARTESIAN_POINT('Ctrl Pts',(159.763883554416,4.18448451454465,339.186031610541));
#9779=CARTESIAN_POINT('Ctrl Pts',(159.756486425953,4.29294518794165,339.071676826054));
#9780=CARTESIAN_POINT('Ctrl Pts',(159.749088158516,4.40142256157498,338.957304433786));
#9781=CARTESIAN_POINT('Ctrl Pts',(159.741689891079,4.50530693030502,338.838614231186));
#9782=CARTESIAN_POINT('Ctrl Pts',(159.734291623643,4.6042507422102,338.716020137911));
#9783=CARTESIAN_POINT('Ctrl Pts',(159.726890757117,4.70322931411653,338.593382976041));
#9784=CARTESIAN_POINT('Ctrl Pts',(159.719489890591,4.7972636392349,338.466839483126));
#9785=CARTESIAN_POINT('Ctrl Pts',(159.712089024066,4.88604790169609,338.336834797354));
#9786=CARTESIAN_POINT('Ctrl Pts',(159.704680030681,4.97492965776604,338.206687354007));
#9787=CARTESIAN_POINT('Ctrl Pts',(159.697271037296,5.0585496274213,338.073071435944));
#9788=CARTESIAN_POINT('Ctrl Pts',(159.689862043911,5.13664622772738,337.936459789215));
#9789=CARTESIAN_POINT('Ctrl Pts',(159.682448486331,5.21479093823327,337.799763984998));
#9790=CARTESIAN_POINT('Ctrl Pts',(159.675034928751,5.28740532755787,337.660069105139));
#9791=CARTESIAN_POINT('Ctrl Pts',(159.66762137117,5.35427508979995,337.517869898396));
#9792=CARTESIAN_POINT('Ctrl Pts',(159.660197259034,5.42124005339057,337.375468245049));
#9793=CARTESIAN_POINT('Ctrl Pts',(159.652773146897,5.48244391092731,337.230555486944));
#9794=CARTESIAN_POINT('Ctrl Pts',(159.64534903476,5.53772124773015,337.08364439023));
#9795=CARTESIAN_POINT('Ctrl Pts',(159.641491909606,5.56644004970121,337.00731816075));
#9796=CARTESIAN_POINT('Ctrl Pts',(159.637634784451,5.5935599811839,336.930452763466));
#9797=CARTESIAN_POINT('Ctrl Pts',(159.633777659296,5.61906326742996,336.853121301782));
#9798=CARTESIAN_POINT('Ctrl Pts',(159.626353681858,5.66815055759916,336.704278056161));
#9799=CARTESIAN_POINT('Ctrl Pts',(159.61892970442,5.71139375593611,336.553258518005));
#9800=CARTESIAN_POINT('Ctrl Pts',(159.611505726982,5.74859595230427,336.400562436898));
#9801=CARTESIAN_POINT('Ctrl Pts',(159.604090510955,5.78575424448335,336.248046560142));
#9802=CARTESIAN_POINT('Ctrl Pts',(159.596675294927,5.81688563817707,336.093858437896));
#9803=CARTESIAN_POINT('Ctrl Pts',(159.589260078899,5.84184210507707,335.938515520303));
#9804=CARTESIAN_POINT('Ctrl Pts',(159.581851997755,5.86677455899026,335.783322072882));
#9805=CARTESIAN_POINT('Ctrl Pts',(159.574443916611,5.88554385569258,335.626976408208));
#9806=CARTESIAN_POINT('Ctrl Pts',(159.567035835467,5.89805242439832,335.470008682419));
#9807=CARTESIAN_POINT('Ctrl Pts',(159.559633268293,5.91055168274794,335.313157790574));
#9808=CARTESIAN_POINT('Ctrl Pts',(159.552230701119,5.91679946226846,335.155686129975));
#9809=CARTESIAN_POINT('Ctrl Pts',(159.544828133945,5.91674970494396,334.9981314322));
#9810=CARTESIAN_POINT('Ctrl Pts',(159.53742946419,5.91669997381647,334.840659686284));
#9811=CARTESIAN_POINT('Ctrl Pts',(159.530030794436,5.91035930922668,334.68310536253));
#9812=CARTESIAN_POINT('Ctrl Pts',(159.522632124681,5.8977336895992,334.526008555914));
#9813=CARTESIAN_POINT('Ctrl Pts',(159.515234675477,5.88511015280691,334.368937665393));
#9814=CARTESIAN_POINT('Ctrl Pts',(159.507837226273,5.86620374860339,334.212324513865));
#9815=CARTESIAN_POINT('Ctrl Pts',(159.500439777069,5.84107250725722,334.056706552835));
#9816=CARTESIAN_POINT('Ctrl Pts',(159.493042648605,5.81594235555791,333.901095339129));
#9817=CARTESIAN_POINT('Ctrl Pts',(159.485645520142,5.78458796286248,333.746479598564));
#9818=CARTESIAN_POINT('Ctrl Pts',(159.478248391679,5.74711887878303,333.593388768836));
#9819=CARTESIAN_POINT('Ctrl Pts',(159.470850124242,5.70964402539995,333.440274366942));
#9820=CARTESIAN_POINT('Ctrl Pts',(159.463451856805,5.66605269469313,333.288685705932));
#9821=CARTESIAN_POINT('Ctrl Pts',(159.456053589369,5.61650488024397,333.139139045308));
#9822=CARTESIAN_POINT('Ctrl Pts',(159.448652722843,5.56693965912644,332.98953984737));
#9823=CARTESIAN_POINT('Ctrl Pts',(159.441251856317,5.51141390525624,332.841984432162));
#9824=CARTESIAN_POINT('Ctrl Pts',(159.433850989791,5.45013645031971,332.69697085659));
#9825=CARTESIAN_POINT('Ctrl Pts',(159.426441996407,5.3887917068794,332.551798042248));
#9826=CARTESIAN_POINT('Ctrl Pts',(159.419033003022,5.32168279450289,332.409172985668));
#9827=CARTESIAN_POINT('Ctrl Pts',(159.411624009637,5.24906569789374,332.269571487533));
#9828=CARTESIAN_POINT('Ctrl Pts',(159.404210452057,5.17640386664838,332.129883990059));
#9829=CARTESIAN_POINT('Ctrl Pts',(159.396796894477,5.09822727459202,331.993224085735));
#9830=CARTESIAN_POINT('Ctrl Pts',(159.389383336897,5.01483599329072,331.860039725905));
#9831=CARTESIAN_POINT('Ctrl Pts',(159.38195922476,4.93132598923354,331.726665753756));
#9832=CARTESIAN_POINT('Ctrl Pts',(159.374535112623,4.84258667855479,331.596777515723));
#9833=CARTESIAN_POINT('Ctrl Pts',(159.367111000487,4.74895974187416,331.470791599727));
#9834=CARTESIAN_POINT('Ctrl Pts',(159.363253875332,4.70031677878593,331.40533684409));
#9835=CARTESIAN_POINT('Ctrl Pts',(159.359396750177,4.65035517742486,331.340934838121));
#9836=CARTESIAN_POINT('Ctrl Pts',(159.355539625023,4.59912679306621,331.277640089432));
#9837=CARTESIAN_POINT('Ctrl Pts',(159.348115647585,4.50052528173033,331.155813919068));
#9838=CARTESIAN_POINT('Ctrl Pts',(159.340691670147,4.3969311061483,331.037724453438));
#9839=CARTESIAN_POINT('Ctrl Pts',(159.333267692709,4.28865795703438,330.923807721652));
#9840=CARTESIAN_POINT('Ctrl Pts',(159.325852476681,4.18051258652741,330.810025428749));
#9841=CARTESIAN_POINT('Ctrl Pts',(159.318437260653,4.06769948851795,330.700406335373));
#9842=CARTESIAN_POINT('Ctrl Pts',(159.311022044626,3.95057369125965,330.59535494365));
#9843=CARTESIAN_POINT('Ctrl Pts',(159.303613963482,3.83356059185371,330.490404631847));
#9844=CARTESIAN_POINT('Ctrl Pts',(159.296205882338,3.71224333036871,330.390013519557));
#9845=CARTESIAN_POINT('Ctrl Pts',(159.288797801194,3.58701492526119,330.294550554043));
#9846=CARTESIAN_POINT('Ctrl Pts',(159.28139523402,3.46187972994267,330.199158643358));
#9847=CARTESIAN_POINT('Ctrl Pts',(159.273992666846,3.33283948303129,330.108687800997));
#9848=CARTESIAN_POINT('Ctrl Pts',(159.266590099672,3.2003214498467,330.02346775554));
#9849=CARTESIAN_POINT('Ctrl Pts',(159.259191429917,3.06787318682628,329.938292578063));
#9850=CARTESIAN_POINT('Ctrl Pts',(159.251792760162,2.93195109727048,329.858362893141));
#9851=CARTESIAN_POINT('Ctrl Pts',(159.244394090408,2.79301259383497,329.783965949768));
#9852=CARTESIAN_POINT('Ctrl Pts',(159.236996641204,2.65409701093913,329.709581279582));
#9853=CARTESIAN_POINT('Ctrl Pts',(159.229599192,2.51216633046017,329.640727715474));
#9854=CARTESIAN_POINT('Ctrl Pts',(159.222201742796,2.36770391034426,329.577647304404));
#9855=CARTESIAN_POINT('Ctrl Pts',(159.214804614332,2.22324775386717,329.51456962839));
#9856=CARTESIAN_POINT('Ctrl Pts',(159.207407485869,2.07626041804183,329.457264757055));
#9857=CARTESIAN_POINT('Ctrl Pts',(159.200010357405,1.92724640190293,329.40592707691));
#9858=CARTESIAN_POINT('Ctrl Pts',(159.192612089969,1.77820944132487,329.354581492043));
#9859=CARTESIAN_POINT('Ctrl Pts',(159.185213822532,1.62714553196356,329.309205049386));
#9860=CARTESIAN_POINT('Ctrl Pts',(159.177815555096,1.47457538915518,329.269942584564));
#9861=CARTESIAN_POINT('Ctrl Pts',(159.17041468857,1.32195164685127,329.230666326424));
#9862=CARTESIAN_POINT('Ctrl Pts',(159.163013822044,1.16782097875985,329.197508415547));
#9863=CARTESIAN_POINT('Ctrl Pts',(159.155612955518,1.0127152223666,329.170562768081));
#9864=CARTESIAN_POINT('Ctrl Pts',(159.148203962134,0.85743914502415,329.143587531718));
#9865=CARTESIAN_POINT('Ctrl Pts',(159.140794968749,0.701186208977727,329.122838245901));
#9866=CARTESIAN_POINT('Ctrl Pts',(159.133385975364,0.544495053184813,329.108357130684));
#9867=CARTESIAN_POINT('Ctrl Pts',(159.125972417784,0.387707370235105,329.093867094601));
#9868=CARTESIAN_POINT('Ctrl Pts',(159.118558860204,0.230481301443147,329.085652942912));
#9869=CARTESIAN_POINT('Ctrl Pts',(159.111145302623,0.0733559245951565,329.083704751212));
#9870=CARTESIAN_POINT('Ctrl Pts',(159.103721190487,-0.083993148992508,329.081753785905));
#9871=CARTESIAN_POINT('Ctrl Pts',(159.09629707835,-0.24124087226726,329.08608658684));
#9872=CARTESIAN_POINT('Ctrl Pts',(159.088872966213,-0.397852024571218,329.096641267122));
#9873=CARTESIAN_POINT('Ctrl Pts',(159.085015841059,-0.479217823460725,329.102124848467));
#9874=CARTESIAN_POINT('Ctrl Pts',(159.081158715904,-0.560411933527618,329.10928700412));
#9875=CARTESIAN_POINT('Ctrl Pts',(159.077301590749,-0.641360456293825,329.118113625069));
#9876=CARTESIAN_POINT('Ctrl Pts',(159.069877613312,-0.797165617537513,329.135102608354));
#9877=CARTESIAN_POINT('Ctrl Pts',(159.062453635874,-0.952530321154162,329.158312174861));
#9878=CARTESIAN_POINT('Ctrl Pts',(159.055029658436,-1.10691814491711,329.187714495747));
#9879=CARTESIAN_POINT('Ctrl Pts',(159.047614442408,-1.26112376781904,329.21708211747));
#9880=CARTESIAN_POINT('Ctrl Pts',(159.04019922638,-1.41435444260713,329.25262787698));
#9881=CARTESIAN_POINT('Ctrl Pts',(159.032784010353,-1.56607788865388,329.294272122755));
#9882=CARTESIAN_POINT('Ctrl Pts',(159.025375929209,-1.71765534716503,329.335876298646));
#9883=CARTESIAN_POINT('Ctrl Pts',(159.017967848064,-1.86772810661278,329.383567180719));
#9884=CARTESIAN_POINT('Ctrl Pts',(159.01055976692,-2.01577322653504,329.437213929901));
#9885=CARTESIAN_POINT('Ctrl Pts',(159.003157199746,-2.16370815376932,329.490820748828));
#9886=CARTESIAN_POINT('Ctrl Pts',(158.995754632573,-2.30961809715199,329.550374481391));
#9887=CARTESIAN_POINT('Ctrl Pts',(158.988352065399,-2.45299456310526,329.615694266122));
#9888=CARTESIAN_POINT('Ctrl Pts',(158.980953395644,-2.59629554197724,329.680979660272));
#9889=CARTESIAN_POINT('Ctrl Pts',(158.973554725889,-2.73706536111975,329.752024906273));
#9890=CARTESIAN_POINT('Ctrl Pts',(158.966156056134,-2.87481493448873,329.82860080298));
#9891=CARTESIAN_POINT('Ctrl Pts',(158.95875860693,-3.01254178345519,329.905164067041));
#9892=CARTESIAN_POINT('Ctrl Pts',(158.951361157726,-3.14724904962742,329.987255989859));
#9893=CARTESIAN_POINT('Ctrl Pts',(158.943963708522,-3.27847161783451,330.074601090921));
#9894=CARTESIAN_POINT('Ctrl Pts',(158.936566580059,-3.40968849645989,330.161942404852));
#9895=CARTESIAN_POINT('Ctrl Pts',(158.929169451595,-3.53742066685793,330.254536237353));
#9896=CARTESIAN_POINT('Ctrl Pts',(158.921772323132,-3.66123165188905,330.352063538117));
#9897=CARTESIAN_POINT('Ctrl Pts',(158.914374055695,-3.78506170072144,330.44960585565));
#9898=CARTESIAN_POINT('Ctrl Pts',(158.906975788259,-3.90496906881592,330.552082923018));
#9899=CARTESIAN_POINT('Ctrl Pts',(158.899577520822,-4.02055017185975,330.659135238451));
#9900=CARTESIAN_POINT('Ctrl Pts',(158.892176654296,-4.13617187976178,330.76622516249));
#9901=CARTESIAN_POINT('Ctrl Pts',(158.88477578777,-4.24746402293306,330.877893281346));
#9902=CARTESIAN_POINT('Ctrl Pts',(158.877374921244,-4.35405981749925,330.993743184949));
#9903=CARTESIAN_POINT('Ctrl Pts',(158.86996592786,-4.46077266443758,331.109720302822));
#9904=CARTESIAN_POINT('Ctrl Pts',(158.862556934475,-4.56277861103342,331.229888101104));
#9905=CARTESIAN_POINT('Ctrl Pts',(158.85514794109,-4.65975066509635,331.353816474499));
#9906=CARTESIAN_POINT('Ctrl Pts',(158.84773438351,-4.75678245728948,331.477821192047));
#9907=CARTESIAN_POINT('Ctrl Pts',(158.84032082593,-4.84877396013921,331.605590798758));
#9908=CARTESIAN_POINT('Ctrl Pts',(158.832907268349,-4.93544179336682,331.736666601956));
#9909=CARTESIAN_POINT('Ctrl Pts',(158.825483156213,-5.0222330141217,331.867929015557));
#9910=CARTESIAN_POINT('Ctrl Pts',(158.818059044076,-5.10368523531542,332.002506707993));
#9911=CARTESIAN_POINT('Ctrl Pts',(158.810634931939,-5.1795608603498,332.139916110246));
#9912=CARTESIAN_POINT('Ctrl Pts',(158.806777806785,-5.21898130235845,332.21130582691));
#9913=CARTESIAN_POINT('Ctrl Pts',(158.80292068163,-5.25689728474739,332.283459539655));
#9914=CARTESIAN_POINT('Ctrl Pts',(158.799063556475,-5.29328068137832,332.356307470479));
#9915=CARTESIAN_POINT('Ctrl Pts',(158.791118272457,-5.36822676381,332.506366770435));
#9916=CARTESIAN_POINT('Ctrl Pts',(158.783172988438,-5.43686838976672,332.65977603528));
#9917=CARTESIAN_POINT('Ctrl Pts',(158.775227704419,-5.49891546224878,332.815999244153));
#9918=CARTESIAN_POINT('Ctrl Pts',(158.767297571479,-5.56084421548026,332.971924546738));
#9919=CARTESIAN_POINT('Ctrl Pts',(158.759367438539,-5.61620338153345,333.13065282336));
#9920=CARTESIAN_POINT('Ctrl Pts',(158.751437305598,-5.66474934606599,333.291624921528));
#9921=CARTESIAN_POINT('Ctrl Pts',(158.743528739818,-5.71316328272739,333.452159232464));
#9922=CARTESIAN_POINT('Ctrl Pts',(158.735620174037,-5.75480089439849,333.614924913133));
#9923=CARTESIAN_POINT('Ctrl Pts',(158.727711608256,-5.78946735267797,333.779345120529));
#9924=CARTESIAN_POINT('Ctrl Pts',(158.719816288477,-5.82407574835078,333.943489941679));
#9925=CARTESIAN_POINT('Ctrl Pts',(158.711920968697,-5.85173620522388,334.109283480948));
#9926=CARTESIAN_POINT('Ctrl Pts',(158.704025648917,-5.87230346456176,334.27613358788));
#9927=CARTESIAN_POINT('Ctrl Pts',(158.696148894247,-5.89282236190352,334.442591362314));
#9928=CARTESIAN_POINT('Ctrl Pts',(158.688272139577,-5.90628129190153,334.610100459849));
#9929=CARTESIAN_POINT('Ctrl Pts',(158.680395384907,-5.91258595816309,334.778058904588));
#9930=CARTESIAN_POINT('Ctrl Pts',(158.676947609815,-5.91534560629397,334.851576865549));
#9931=CARTESIAN_POINT('Ctrl Pts',(158.673499834723,-5.91673518973076,334.925180763386));
#9932=CARTESIAN_POINT('Ctrl Pts',(158.67005205963,-5.91674988223068,334.998819481802));
#9933=CARTESIAN_POINT('',(156.920052004703,-5.91590632165756,335.005448065324));
#9934=CARTESIAN_POINT('Ctrl Pts',(158.670052004703,-5.90718086102098,334.998822562282));
#9935=CARTESIAN_POINT('Ctrl Pts',(158.620309843869,-5.90529945334112,336.059514263974));
#9936=CARTESIAN_POINT('Ctrl Pts',(158.477821671611,-5.12528683190018,339.100484283673));
#9937=CARTESIAN_POINT('Ctrl Pts',(158.242587487927,-0.252042696482904,341.992073898377));
#9938=CARTESIAN_POINT('Ctrl Pts',(157.964349453653,5.74338934522624,338.995760472095));
#9939=CARTESIAN_POINT('Ctrl Pts',(157.686111419379,6.46819775710926,332.3325966379));
#9940=CARTESIAN_POINT('Ctrl Pts',(157.407873385105,1.25723655773474,328.117269498293));
#9941=CARTESIAN_POINT('Ctrl Pts',(157.15252024688,-4.5839789583817,330.045328763812));
#9942=CARTESIAN_POINT('Ctrl Pts',(156.989913120079,-5.90237610370384,333.521276051786));
#9943=CARTESIAN_POINT('Ctrl Pts',(156.920052004703,-5.91590632165756,335.005448065324));
#9944=CARTESIAN_POINT('',(155.170051131044,-5.92181705319278,334.998466635511));
#9945=CARTESIAN_POINT('Ctrl Pts',(156.920051980179,-5.91674749055292,335.005449361037));
#9946=CARTESIAN_POINT('Ctrl Pts',(156.910500549411,-5.91656057844607,335.208392739462));
#9947=CARTESIAN_POINT('Ctrl Pts',(156.900949118643,-5.90592887574173,335.410870699688));
#9948=CARTESIAN_POINT('Ctrl Pts',(156.891397687875,-5.88501638256968,335.61197445975));
#9949=CARTESIAN_POINT('Ctrl Pts',(156.88162723986,-5.86362435949407,335.817689590914));
#9950=CARTESIAN_POINT('Ctrl Pts',(156.871856791845,-5.83147464020149,336.021967055827));
#9951=CARTESIAN_POINT('Ctrl Pts',(156.86208634383,-5.78879070814869,336.223859754936));
#9952=CARTESIAN_POINT('Ctrl Pts',(156.858523334739,-5.77322507208986,336.29748437493));
#9953=CARTESIAN_POINT('Ctrl Pts',(156.854960325648,-5.75625899132762,336.370792075941));
#9954=CARTESIAN_POINT('Ctrl Pts',(156.851397316557,-5.73790486259783,336.443737632077));
#9955=CARTESIAN_POINT('Ctrl Pts',(156.843973339119,-5.69966172762065,336.595728870147));
#9956=CARTESIAN_POINT('Ctrl Pts',(156.836549361681,-5.65531759153176,336.746428812752));
#9957=CARTESIAN_POINT('Ctrl Pts',(156.829125384243,-5.60497375020673,336.895309954069));
#9958=CARTESIAN_POINT('Ctrl Pts',(156.821710168216,-5.55468932218909,337.044015393239));
#9959=CARTESIAN_POINT('Ctrl Pts',(156.814294952188,-5.49841940128052,337.190905953574));
#9960=CARTESIAN_POINT('Ctrl Pts',(156.80687973616,-5.43631604491004,337.335465354561));
#9961=CARTESIAN_POINT('Ctrl Pts',(156.799471655016,-5.37427244407629,337.479885661219));
#9962=CARTESIAN_POINT('Ctrl Pts',(156.792063573872,-5.30640672835238,337.621978933368));
#9963=CARTESIAN_POINT('Ctrl Pts',(156.784655492728,-5.23292037307704,337.76124517773));
#9964=CARTESIAN_POINT('Ctrl Pts',(156.777252925554,-5.15948871503811,337.900407763682));
#9965=CARTESIAN_POINT('Ctrl Pts',(156.76985035838,-5.0804449209197,338.036747182969));
#9966=CARTESIAN_POINT('Ctrl Pts',(156.762447791207,-4.99603802795934,338.16978462765));
#9967=CARTESIAN_POINT('Ctrl Pts',(156.755049121452,-4.91167557485941,338.302752028697));
#9968=CARTESIAN_POINT('Ctrl Pts',(156.747650451697,-4.82195584581747,338.432420603074));
#9969=CARTESIAN_POINT('Ctrl Pts',(156.740251781943,-4.72717309138047,338.558337410453));
#9970=CARTESIAN_POINT('Ctrl Pts',(156.732854332739,-4.63240597315461,338.684233445469));
#9971=CARTESIAN_POINT('Ctrl Pts',(156.725456883535,-4.53257771145043,338.806378643967));
#9972=CARTESIAN_POINT('Ctrl Pts',(156.718059434331,-4.42802510213637,338.924350170073));
#9973=CARTESIAN_POINT('Ctrl Pts',(156.710662305868,-4.32347702604129,339.042316581139));
#9974=CARTESIAN_POINT('Ctrl Pts',(156.703265177404,-4.21420525716126,339.156109400319));
#9975=CARTESIAN_POINT('Ctrl Pts',(156.695868048941,-4.10058581133365,339.265340146622));
#9976=CARTESIAN_POINT('Ctrl Pts',(156.688469781504,-3.98694887094747,339.374587711734));
#9977=CARTESIAN_POINT('Ctrl Pts',(156.681071514068,-3.86896318974458,339.479271546638));
#9978=CARTESIAN_POINT('Ctrl Pts',(156.673673246631,-3.74704032997384,339.579041311022));
#9979=CARTESIAN_POINT('Ctrl Pts',(156.666272380106,-3.62507463742024,339.678846125574));
#9980=CARTESIAN_POINT('Ctrl Pts',(156.65887151358,-3.49916930105579,339.773733196214));
#9981=CARTESIAN_POINT('Ctrl Pts',(156.651470647054,-3.36976738290881,339.863393706825));
#9982=CARTESIAN_POINT('Ctrl Pts',(156.64406165367,-3.24022336908449,339.953152673249));
#9983=CARTESIAN_POINT('Ctrl Pts',(156.636652660285,-3.10717541258079,340.037673405348));
#9984=CARTESIAN_POINT('Ctrl Pts',(156.6292436669,-2.97109448148061,340.116691132423));
#9985=CARTESIAN_POINT('Ctrl Pts',(156.62183010932,-2.83492971983294,340.195757537143));
#9986=CARTESIAN_POINT('Ctrl Pts',(156.61441655174,-2.69572858972507,340.269314007776));
#9987=CARTESIAN_POINT('Ctrl Pts',(156.60700299416,-2.55398438083638,340.33714290093));
#9988=CARTESIAN_POINT('Ctrl Pts',(156.599578882023,-2.41203837311668,340.405068360931));
#9989=CARTESIAN_POINT('Ctrl Pts',(156.592154769887,-2.26754239756873,340.467249810648));
#9990=CARTESIAN_POINT('Ctrl Pts',(156.58473065775,-2.12100809114677,340.523518375075));
#9991=CARTESIAN_POINT('Ctrl Pts',(156.580873532595,-2.04487761937375,340.552752159712));
#9992=CARTESIAN_POINT('Ctrl Pts',(156.577016407439,-1.96819719059255,340.580390752808));
#9993=CARTESIAN_POINT('Ctrl Pts',(156.573159282284,-1.89103978645724,340.606415886155));
#9994=CARTESIAN_POINT('Ctrl Pts',(156.565735304846,-1.74253155704533,340.656507598247));
#9995=CARTESIAN_POINT('Ctrl Pts',(156.558311327408,-1.59180760376044,340.700770054274));
#9996=CARTESIAN_POINT('Ctrl Pts',(156.55088734997,-1.43936633451521,340.73900297243));
#9997=CARTESIAN_POINT('Ctrl Pts',(156.543472133942,-1.28710496890372,340.777190769991));
#9998=CARTESIAN_POINT('Ctrl Pts',(156.536056917914,-1.13313067997221,340.809363103809));
#9999=CARTESIAN_POINT('Ctrl Pts',(156.528641701887,-0.977959906019541,340.83536845321));
#10000=CARTESIAN_POINT('Ctrl Pts',(156.521233620743,-0.822938436604197,
340.861348780395));
#10001=CARTESIAN_POINT('Ctrl Pts',(156.513825539599,-0.666723139713503,
340.881173875061));
#10002=CARTESIAN_POINT('Ctrl Pts',(156.506417458454,-0.509843500227656,
340.894742587067));
#10003=CARTESIAN_POINT('Ctrl Pts',(156.49901489128,-0.35308062912281,340.908301199632));
#10004=CARTESIAN_POINT('Ctrl Pts',(156.491612324106,-0.195654770239612,
340.915612669762));
#10005=CARTESIAN_POINT('Ctrl Pts',(156.484209756932,-0.0381033317290172,
340.916627307733));
#10006=CARTESIAN_POINT('Ctrl Pts',(156.476811087178,0.119365156638028,340.917641411501));
#10007=CARTESIAN_POINT('Ctrl Pts',(156.469412417423,0.276958720692679,340.912365283239));
#10008=CARTESIAN_POINT('Ctrl Pts',(156.462013747668,0.434137237396164,340.900801252509));
#10009=CARTESIAN_POINT('Ctrl Pts',(156.454616298464,0.59128982452499,340.889239129484));
#10010=CARTESIAN_POINT('Ctrl Pts',(156.44721884926,0.748027128349952,340.871391190071));
#10011=CARTESIAN_POINT('Ctrl Pts',(156.439821400056,0.903811317593196,340.847311832346));
#10012=CARTESIAN_POINT('Ctrl Pts',(156.432424271593,1.05958875230547,340.82323351866));
#10013=CARTESIAN_POINT('Ctrl Pts',(156.425027143129,1.21441278577318,340.792924380886));
#10014=CARTESIAN_POINT('Ctrl Pts',(156.417630014666,1.36775325229648,340.756490389407));
#10015=CARTESIAN_POINT('Ctrl Pts',(156.410231747229,1.52111732942384,340.720050788003));
#10016=CARTESIAN_POINT('Ctrl Pts',(156.402833479792,1.67299702164339,340.677484541387));
#10017=CARTESIAN_POINT('Ctrl Pts',(156.395435212356,1.822875000364,340.628948151791));
#10018=CARTESIAN_POINT('Ctrl Pts',(156.38803434583,1.97280563279464,340.58039471085));
#10019=CARTESIAN_POINT('Ctrl Pts',(156.380633479304,2.12073279677664,340.525867065969));
#10020=CARTESIAN_POINT('Ctrl Pts',(156.373232612778,2.26615703596342,340.465570679339));
#10021=CARTESIAN_POINT('Ctrl Pts',(156.365823619394,2.41174096486809,340.405208081513));
#10022=CARTESIAN_POINT('Ctrl Pts',(156.358414626009,2.55481613521681,340.339064234371));
#10023=CARTESIAN_POINT('Ctrl Pts',(156.351005632624,2.69490502782445,340.267391902404));
#10024=CARTESIAN_POINT('Ctrl Pts',(156.343592075044,2.83508022002213,340.195675417808));
#10025=CARTESIAN_POINT('Ctrl Pts',(156.336178517463,2.97226514429686,340.1184238447));
#10026=CARTESIAN_POINT('Ctrl Pts',(156.328764959883,3.10600983232754,340.03593422157));
#10027=CARTESIAN_POINT('Ctrl Pts',(156.321340847746,3.23994493040673,339.95332715936));
#10028=CARTESIAN_POINT('Ctrl Pts',(156.31391673561,3.37042970160363,339.865467361246));
#10029=CARTESIAN_POINT('Ctrl Pts',(156.306492623473,3.49704525920953,339.772693685702));
#10030=CARTESIAN_POINT('Ctrl Pts',(156.302635498318,3.56282713901046,339.724494026128));
#10031=CARTESIAN_POINT('Ctrl Pts',(156.298778373164,3.62756520150735,339.6749686463));
#10032=CARTESIAN_POINT('Ctrl Pts',(156.294921248009,3.69120459001352,339.624169032071));
#10033=CARTESIAN_POINT('Ctrl Pts',(156.287497270571,3.81369410370632,339.526392793349));
#10034=CARTESIAN_POINT('Ctrl Pts',(156.280073293133,3.932480726939,339.423598760212));
#10035=CARTESIAN_POINT('Ctrl Pts',(156.272649315695,4.04712632134682,339.316097670531));
#10036=CARTESIAN_POINT('Ctrl Pts',(156.265234099668,4.16163661670388,339.208723448309));
#10037=CARTESIAN_POINT('Ctrl Pts',(156.25781888364,4.27201534136185,339.096653479727));
#10038=CARTESIAN_POINT('Ctrl Pts',(156.250403667612,4.37785560395626,338.980240052234));
#10039=CARTESIAN_POINT('Ctrl Pts',(156.242995586468,4.48359402758291,338.863938637156));
#10040=CARTESIAN_POINT('Ctrl Pts',(156.235587505324,4.58480243341674,338.74330235758));
#10041=CARTESIAN_POINT('Ctrl Pts',(156.22817942418,4.68110922749544,338.618721730495));
#10042=CARTESIAN_POINT('Ctrl Pts',(156.220776857006,4.77734433866842,338.494233831046));
#10043=CARTESIAN_POINT('Ctrl Pts',(156.213374289832,4.86868487522002,338.365807723797));
#10044=CARTESIAN_POINT('Ctrl Pts',(156.205971722658,4.95479822961385,338.233868436767));
#10045=CARTESIAN_POINT('Ctrl Pts',(156.198573052903,5.04086624570299,338.101998615194));
#10046=CARTESIAN_POINT('Ctrl Pts',(156.191174383148,5.1217123571128,337.966619609323));
#10047=CARTESIAN_POINT('Ctrl Pts',(156.183775713394,5.19704623125318,337.828186880798));
#10048=CARTESIAN_POINT('Ctrl Pts',(156.17637826419,5.27236767764358,337.689776989375));
#10049=CARTESIAN_POINT('Ctrl Pts',(156.168980814986,5.34217851330621,337.548314702613));
#10050=CARTESIAN_POINT('Ctrl Pts',(156.161583365782,5.40623343137915,337.404281732231));
#10051=CARTESIAN_POINT('Ctrl Pts',(156.154186237318,5.47028557214251,337.260255006866));
#10052=CARTESIAN_POINT('Ctrl Pts',(156.146789108855,5.52858213988165,337.11365816051));
#10053=CARTESIAN_POINT('Ctrl Pts',(156.139391980391,5.5809253442718,336.964994367464));
#10054=CARTESIAN_POINT('Ctrl Pts',(156.131993712955,5.63327660820878,336.816307683905));
#10055=CARTESIAN_POINT('Ctrl Pts',(156.124595445518,5.67967255963381,336.665553772012));
#10056=CARTESIAN_POINT('Ctrl Pts',(156.117197178081,5.71996484842579,336.513252356771));
#10057=CARTESIAN_POINT('Ctrl Pts',(156.109796311556,5.76027129232258,336.360897436441));
#10058=CARTESIAN_POINT('Ctrl Pts',(156.10239544503,5.79446970893535,336.20699429092));
#10059=CARTESIAN_POINT('Ctrl Pts',(156.094994578504,5.82246259131658,336.052074111087));
#10060=CARTESIAN_POINT('Ctrl Pts',(156.087585585119,5.85048621255889,335.896983814085));
#10061=CARTESIAN_POINT('Ctrl Pts',(156.080176591735,5.87229062470748,335.740874619942));
#10062=CARTESIAN_POINT('Ctrl Pts',(156.07276759835,5.88782996978299,335.584284870098));
#10063=CARTESIAN_POINT('Ctrl Pts',(156.06535404077,5.90337888763107,335.427598655566));
#10064=CARTESIAN_POINT('Ctrl Pts',(156.057940483189,5.91265502590962,335.270431667129));
#10065=CARTESIAN_POINT('Ctrl Pts',(156.050526925609,5.91566466694261,335.113323037317));
#10066=CARTESIAN_POINT('Ctrl Pts',(156.043102813472,5.9186785927506,334.955990734608));
#10067=CARTESIAN_POINT('Ctrl Pts',(156.035678701336,5.91540821101888,334.798717328585));
#10068=CARTESIAN_POINT('Ctrl Pts',(156.028254589199,5.90591179143411,334.64203844578));
#10069=CARTESIAN_POINT('Ctrl Pts',(156.024397464045,5.90097801912786,334.560637458171));
#10070=CARTESIAN_POINT('Ctrl Pts',(156.02054033889,5.89436455093886,334.479396815501));
#10071=CARTESIAN_POINT('Ctrl Pts',(156.016683213735,5.88608499631948,334.39839050988));
#10072=CARTESIAN_POINT('Ctrl Pts',(156.009259236297,5.87014897551951,334.242474131445));
#10073=CARTESIAN_POINT('Ctrl Pts',(156.001835258859,5.84798953784702,334.086956176117));
#10074=CARTESIAN_POINT('Ctrl Pts',(155.994411281421,5.81963088759558,333.932373241885));
#10075=CARTESIAN_POINT('Ctrl Pts',(155.986996065394,5.79130570481823,333.777972738774));
#10076=CARTESIAN_POINT('Ctrl Pts',(155.979580849366,5.75679593877136,333.624505423809));
#10077=CARTESIAN_POINT('Ctrl Pts',(155.972165633339,5.71617764322439,333.472504103573));
#10078=CARTESIAN_POINT('Ctrl Pts',(155.964757552194,5.67559843039689,333.320649038242));
#10079=CARTESIAN_POINT('Ctrl Pts',(155.95734947105,5.62892248497393,333.170257517604));
#10080=CARTESIAN_POINT('Ctrl Pts',(155.949941389906,5.5762771102056,333.021853354097));
#10081=CARTESIAN_POINT('Ctrl Pts',(155.942538822732,5.52367092035119,332.87355965052));
#10082=CARTESIAN_POINT('Ctrl Pts',(155.935136255558,5.46510427236193,332.727250708948));
#10083=CARTESIAN_POINT('Ctrl Pts',(155.927733688384,5.40075458834285,332.583436233203));
#10084=CARTESIAN_POINT('Ctrl Pts',(155.92033501863,5.33643878415119,332.439697475152));
#10085=CARTESIAN_POINT('Ctrl Pts',(155.912936348875,5.26634615976231,332.298450907169));
#10086=CARTESIAN_POINT('Ctrl Pts',(155.90553767912,5.19070260696743,332.160187152554));
#10087=CARTESIAN_POINT('Ctrl Pts',(155.898140229916,5.11507153300986,332.021946207164));
#10088=CARTESIAN_POINT('Ctrl Pts',(155.890742780712,5.03389152702902,331.886687425636));
#10089=CARTESIAN_POINT('Ctrl Pts',(155.883345331508,4.94743492106539,331.754877773593));
#10090=CARTESIAN_POINT('Ctrl Pts',(155.875948203045,4.86098206370951,331.623073836586));
#10091=CARTESIAN_POINT('Ctrl Pts',(155.868551074581,4.769253265962,331.494719043783));
#10092=CARTESIAN_POINT('Ctrl Pts',(155.861153946118,4.67256462213479,331.370252017774));
#10093=CARTESIAN_POINT('Ctrl Pts',(155.853755678681,4.57586109067005,331.24576582695));
#10094=CARTESIAN_POINT('Ctrl Pts',(155.846357411244,4.47419642148117,331.1251688896));
#10095=CARTESIAN_POINT('Ctrl Pts',(155.838959143808,4.36792738163358,331.008867209516));
#10096=CARTESIAN_POINT('Ctrl Pts',(155.831558277282,4.2616210083546,330.892524671429));
#10097=CARTESIAN_POINT('Ctrl Pts',(155.824157410756,4.15070729544045,330.780480670306));
#10098=CARTESIAN_POINT('Ctrl Pts',(155.816756544231,4.03558016602919,330.673104659684));
#10099=CARTESIAN_POINT('Ctrl Pts',(155.809347550846,3.9203266160233,330.565610739936));
#10100=CARTESIAN_POINT('Ctrl Pts',(155.801938557461,3.80085068277585,330.462795302089));
#10101=CARTESIAN_POINT('Ctrl Pts',(155.794529564076,3.67758025270406,330.364988236539));
#10102=CARTESIAN_POINT('Ctrl Pts',(155.787116006496,3.55423388379526,330.267120918463));
#10103=CARTESIAN_POINT('Ctrl Pts',(155.779702448916,3.42708866089523,330.174268340203));
#10104=CARTESIAN_POINT('Ctrl Pts',(155.772288891336,3.29660135177702,330.086716974368));
#10105=CARTESIAN_POINT('Ctrl Pts',(155.764864779199,3.16592827008551,329.999040963135));
#10106=CARTESIAN_POINT('Ctrl Pts',(155.757440667062,3.03190391646984,329.916681432558));
#10107=CARTESIAN_POINT('Ctrl Pts',(155.750016554925,2.89501024378064,329.839879240666));
#10108=CARTESIAN_POINT('Ctrl Pts',(155.746159429771,2.82388846938806,329.799977409871));
#10109=CARTESIAN_POINT('Ctrl Pts',(155.742302304616,2.75199255265327,329.761574843026));
#10110=CARTESIAN_POINT('Ctrl Pts',(155.738445179461,2.6793920799741,329.724700137028));
#10111=CARTESIAN_POINT('Ctrl Pts',(155.731021202023,2.53965477575423,329.653725778048));
#10112=CARTESIAN_POINT('Ctrl Pts',(155.723597224585,2.39688466605584,329.588200432691));
#10113=CARTESIAN_POINT('Ctrl Pts',(155.716173247147,2.25154608590787,329.528394131013));
#10114=CARTESIAN_POINT('Ctrl Pts',(155.70875803112,2.10637902715177,329.468658409769));
#10115=CARTESIAN_POINT('Ctrl Pts',(155.701342815092,1.95864987333785,329.414628438191));
#10116=CARTESIAN_POINT('Ctrl Pts',(155.693927599064,1.80884782994775,329.366528593257));
#10117=CARTESIAN_POINT('Ctrl Pts',(155.68651951792,1.65918992532954,329.318475029751));
#10118=CARTESIAN_POINT('Ctrl Pts',(155.679111436776,1.50746345482844,329.276340346764));
#10119=CARTESIAN_POINT('Ctrl Pts',(155.671703355632,1.35417779459332,329.240300957244));
#10120=CARTESIAN_POINT('Ctrl Pts',(155.664300788458,1.20100622767464,329.204288392499));
#10121=CARTESIAN_POINT('Ctrl Pts',(155.656898221284,1.04627814356175,329.174362172768));
#10122=CARTESIAN_POINT('Ctrl Pts',(155.64949565411,0.890518176354073,329.150648930002));
#10123=CARTESIAN_POINT('Ctrl Pts',(155.642096984355,0.734840216088303,329.126948172155));
#10124=CARTESIAN_POINT('Ctrl Pts',(155.6346983146,0.578131822736678,329.109453932702));
#10125=CARTESIAN_POINT('Ctrl Pts',(155.627299644846,0.420927814909075,329.098241758837));
#10126=CARTESIAN_POINT('Ctrl Pts',(155.619902195642,0.263749740861374,329.087031434632));
#10127=CARTESIAN_POINT('Ctrl Pts',(155.612504746438,0.106076586510544,329.082101145729));
#10128=CARTESIAN_POINT('Ctrl Pts',(155.605107297234,-0.0515515922944678,
329.083474584198));
#10129=CARTESIAN_POINT('Ctrl Pts',(155.59771016877,-0.209172936616341,329.084847963117));
#10130=CARTESIAN_POINT('Ctrl Pts',(155.590313040307,-0.36674893607263,329.092524522709));
#10131=CARTESIAN_POINT('Ctrl Pts',(155.582915911843,-0.523739686799201,
329.106475816375));
#10132=CARTESIAN_POINT('Ctrl Pts',(155.575517644407,-0.680754610182395,
329.120429258192));
#10133=CARTESIAN_POINT('Ctrl Pts',(155.56811937697,-0.837183733638758,329.140659324783));
#10134=CARTESIAN_POINT('Ctrl Pts',(155.560721109533,-0.992492572786399,
329.167085715059));
#10135=CARTESIAN_POINT('Ctrl Pts',(155.553320243008,-1.14785597356264,329.193521389205));
#10136=CARTESIAN_POINT('Ctrl Pts',(155.545919376482,-1.30209793874623,329.226157658543));
#10137=CARTESIAN_POINT('Ctrl Pts',(155.538518509956,-1.45469461256303,329.264863197213));
#10138=CARTESIAN_POINT('Ctrl Pts',(155.531109516571,-1.60745885211655,329.303611238265));
#10139=CARTESIAN_POINT('Ctrl Pts',(155.523700523187,-1.75857383028098,329.348441766472));
#10140=CARTESIAN_POINT('Ctrl Pts',(155.516291529802,-1.90753058129199,329.399173485642));
#10141=CARTESIAN_POINT('Ctrl Pts',(155.508877972222,-2.05657909479966,329.4499364573));
#10142=CARTESIAN_POINT('Ctrl Pts',(155.501464414641,-2.20346638448349,329.506607729786));
#10143=CARTESIAN_POINT('Ctrl Pts',(155.494050857061,-2.3477043661648,329.568958224098));
#10144=CARTESIAN_POINT('Ctrl Pts',(155.486626744924,-2.49214769701924,329.631397485754));
#10145=CARTESIAN_POINT('Ctrl Pts',(155.479202632788,-2.63393385140219,329.69953195621));
#10146=CARTESIAN_POINT('Ctrl Pts',(155.471778520651,-2.77259947431645,329.773086693131));
#10147=CARTESIAN_POINT('Ctrl Pts',(155.467921395497,-2.84464184818796,329.811301340323));
#10148=CARTESIAN_POINT('Ctrl Pts',(155.464064270342,-2.91584239185996,329.850978318078));
#10149=CARTESIAN_POINT('Ctrl Pts',(155.460207145187,-2.98613940039932,329.892074585129));
#10150=CARTESIAN_POINT('Ctrl Pts',(155.452783167749,-3.12144312647544,329.97117436726));
#10151=CARTESIAN_POINT('Ctrl Pts',(155.445359190311,-3.25380588581258,330.055773274156));
#10152=CARTESIAN_POINT('Ctrl Pts',(155.437935212873,-3.38274932604893,330.145626965342));
#10153=CARTESIAN_POINT('Ctrl Pts',(155.430519996846,-3.51154059362524,330.235374615653));
#10154=CARTESIAN_POINT('Ctrl Pts',(155.423104780818,-3.63692027122958,330.330364494898));
#10155=CARTESIAN_POINT('Ctrl Pts',(155.415689564791,-3.75843493831792,330.430306643009));
#10156=CARTESIAN_POINT('Ctrl Pts',(155.408281483646,-3.8798326846054,330.530152627287));
#10157=CARTESIAN_POINT('Ctrl Pts',(155.400873402502,-3.99737253768446,330.634941158621));
#10158=CARTESIAN_POINT('Ctrl Pts',(155.393465321358,-4.1106304954809,330.74433935891));
#10159=CARTESIAN_POINT('Ctrl Pts',(155.386062754184,-4.22380415331075,330.85365613212));
#10160=CARTESIAN_POINT('Ctrl Pts',(155.37866018701,-4.33270199453921,330.967575484366));
#10161=CARTESIAN_POINT('Ctrl Pts',(155.371257619836,-4.43693362204194,331.085724767458));
#10162=CARTESIAN_POINT('Ctrl Pts',(155.363858950082,-4.54111037204843,331.203811845468));
#10163=CARTESIAN_POINT('Ctrl Pts',(155.356460280327,-4.6406255547957,331.326124139877));
#10164=CARTESIAN_POINT('Ctrl Pts',(155.349061610572,-4.7351262199996,331.452252793226));
#10165=CARTESIAN_POINT('Ctrl Pts',(155.341664161368,-4.8296112955282,331.578360639264));
#10166=CARTESIAN_POINT('Ctrl Pts',(155.334266712164,-4.919083271753,331.708283296341));
#10167=CARTESIAN_POINT('Ctrl Pts',(155.32686926296,-5.00322997029795,331.841579441111));
#10168=CARTESIAN_POINT('Ctrl Pts',(155.319472134497,-5.08737302038871,331.974869806392));
#10169=CARTESIAN_POINT('Ctrl Pts',(155.312075006033,-5.16619105267054,332.111533052947));
#10170=CARTESIAN_POINT('Ctrl Pts',(155.30467787757,-5.23941581553427,332.251099770012));
#10171=CARTESIAN_POINT('Ctrl Pts',(155.297279610133,-5.3126518531836,332.390687976867));
#10172=CARTESIAN_POINT('Ctrl Pts',(155.289881342697,-5.38029273320159,332.533180213883));
#10173=CARTESIAN_POINT('Ctrl Pts',(155.28248307526,-5.4421167423182,332.678083566215));
#10174=CARTESIAN_POINT('Ctrl Pts',(155.275082208734,-5.50396247085949,332.823037824619));
#10175=CARTESIAN_POINT('Ctrl Pts',(155.267681342209,-5.55998711347135,332.970404541758));
#10176=CARTESIAN_POINT('Ctrl Pts',(155.260280475683,-5.61001761645535,333.119672128175));
#10177=CARTESIAN_POINT('Ctrl Pts',(155.252871482298,-5.66010305771464,333.269103624673));
#10178=CARTESIAN_POINT('Ctrl Pts',(155.245462488913,-5.70418109578791,333.420439804896));
#10179=CARTESIAN_POINT('Ctrl Pts',(155.238053495529,-5.74212875593335,333.573154558902));
#10180=CARTESIAN_POINT('Ctrl Pts',(155.230639937948,-5.7800997931464,333.725963390464));
#10181=CARTESIAN_POINT('Ctrl Pts',(155.223226380368,-5.81193285192409,333.8801521234));
#10182=CARTESIAN_POINT('Ctrl Pts',(155.215812822788,-5.83755643932879,334.035186349521));
#10183=CARTESIAN_POINT('Ctrl Pts',(155.208388710651,-5.86321650660119,334.190441295245));
#10184=CARTESIAN_POINT('Ctrl Pts',(155.200964598515,-5.88264940063449,334.346543768859));
#10185=CARTESIAN_POINT('Ctrl Pts',(155.193540486378,-5.89583557832674,334.502955338187));
#10186=CARTESIAN_POINT('Ctrl Pts',(155.189683361223,-5.90268632852227,334.584217445688));
#10187=CARTESIAN_POINT('Ctrl Pts',(155.185826236068,-5.90785181112512,334.665562991191));
#10188=CARTESIAN_POINT('Ctrl Pts',(155.181969110914,-5.91133482837328,334.746916793601));
#10189=CARTESIAN_POINT('Ctrl Pts',(155.177996742177,-5.91492191156897,334.830701293287));
#10190=CARTESIAN_POINT('Ctrl Pts',(155.17402437344,-5.91672781384456,334.914562595738));
#10191=CARTESIAN_POINT('Ctrl Pts',(155.170052004703,-5.91674979683974,334.998449484974));
#10192=CARTESIAN_POINT('',(153.420053188954,-5.91355359401508,334.995357850205));
#10193=CARTESIAN_POINT('Ctrl Pts',(155.170050408738,-5.92600646020268,334.998480814896));
#10194=CARTESIAN_POINT('Ctrl Pts',(155.081277298038,-5.91942332648537,336.876090608429));
#10195=CARTESIAN_POINT('Ctrl Pts',(154.899758175916,-3.93940018579113,340.727255971215));
#10196=CARTESIAN_POINT('Ctrl Pts',(154.625493042366,2.62364521063082,341.486070361163));
#10197=CARTESIAN_POINT('Ctrl Pts',(154.347255008092,6.87407990914849,336.303705612426));
#10198=CARTESIAN_POINT('Ctrl Pts',(154.069016973818,4.816272936292,329.924949465835));
#10199=CARTESIAN_POINT('Ctrl Pts',(153.790778939544,-1.66135662212457,328.203492286818));
#10200=CARTESIAN_POINT('Ctrl Pts',(153.574457964201,-5.51217327151609,331.714221820233));
#10201=CARTESIAN_POINT('Ctrl Pts',(153.450883000283,-5.91599721235804,334.339080779984));
#10202=CARTESIAN_POINT('Ctrl Pts',(153.420054047789,-5.91123682344908,334.995341376946));
#10203=CARTESIAN_POINT('',(151.670050828726,-5.91258510326799,335.00367452382));
#10204=CARTESIAN_POINT('Ctrl Pts',(153.420052004703,-5.91674819671435,334.995380565238));
#10205=CARTESIAN_POINT('Ctrl Pts',(153.412312457465,-5.91687694484536,335.160286081005));
#10206=CARTESIAN_POINT('Ctrl Pts',(153.404572910228,-5.91010641488316,335.325274474005));
#10207=CARTESIAN_POINT('Ctrl Pts',(153.39683336299,-5.89644802442704,335.489725696416));
#10208=CARTESIAN_POINT('Ctrl Pts',(153.389442957064,-5.88340578220499,335.646758304562));
#10209=CARTESIAN_POINT('Ctrl Pts',(153.382052551138,-5.86408354313905,335.803300738551));
#10210=CARTESIAN_POINT('Ctrl Pts',(153.374662145212,-5.83854450795694,335.958816244703));
#10211=CARTESIAN_POINT('Ctrl Pts',(153.367271414372,-5.81300434996728,336.114338587995));
#10212=CARTESIAN_POINT('Ctrl Pts',(153.359880683532,-5.78124691155268,336.268833544905));
#10213=CARTESIAN_POINT('Ctrl Pts',(153.352489952691,-5.74338682147282,336.421772971129));
#10214=CARTESIAN_POINT('Ctrl Pts',(153.345097436661,-5.70551758649693,336.574749339027));
#10215=CARTESIAN_POINT('Ctrl Pts',(153.33770492063,-5.6615428544831,336.726169065647));
#10216=CARTESIAN_POINT('Ctrl Pts',(153.3303124046,-5.61162754100708,336.875517769447));
#10217=CARTESIAN_POINT('Ctrl Pts',(153.322916642304,-5.56169030829144,337.024932056527));
#10218=CARTESIAN_POINT('Ctrl Pts',(153.315520880009,-5.50580741819643,337.172273156199));
#10219=CARTESIAN_POINT('Ctrl Pts',(153.308125117713,-5.44419240269467,337.317045455951));
#10220=CARTESIAN_POINT('Ctrl Pts',(153.300720589961,-5.38250436108227,337.461989339818));
#10221=CARTESIAN_POINT('Ctrl Pts',(153.293316062208,-5.31507077499611,337.604358001018));
#10222=CARTESIAN_POINT('Ctrl Pts',(153.285911534456,-5.24215205157905,337.743678631076));
#10223=CARTESIAN_POINT('Ctrl Pts',(153.27850187318,-5.1691827739551,337.88309585147));
#10224=CARTESIAN_POINT('Ctrl Pts',(153.271092211903,-5.09072096791304,338.019460507959));
#10225=CARTESIAN_POINT('Ctrl Pts',(153.263682550627,-5.00707077070543,338.152328164968));
#10226=CARTESIAN_POINT('Ctrl Pts',(153.256262281163,-4.9233008140486,338.285386044569));
#10227=CARTESIAN_POINT('Ctrl Pts',(153.248842011699,-4.83432784604431,338.414936622404));
#10228=CARTESIAN_POINT('Ctrl Pts',(153.241421742236,-4.74049713056373,338.540567400519));
#10229=CARTESIAN_POINT('Ctrl Pts',(153.239048785156,-4.71049063798626,338.58074335987));
#10230=CARTESIAN_POINT('Ctrl Pts',(153.236675828076,-4.6799876412276,338.620518724397));
#10231=CARTESIAN_POINT('Ctrl Pts',(153.234302870997,-4.64900022323675,338.659880802273));
#10232=CARTESIAN_POINT('Ctrl Pts',(153.226878893559,-4.55205371965221,338.783028068852));
#10233=CARTESIAN_POINT('Ctrl Pts',(153.219454916121,-4.45006452049861,338.902506428246));
#10234=CARTESIAN_POINT('Ctrl Pts',(153.212030938683,-4.34334039661702,339.017875652831));
#10235=CARTESIAN_POINT('Ctrl Pts',(153.204615722655,-4.23674222325905,339.133108724374));
#10236=CARTESIAN_POINT('Ctrl Pts',(153.197200506627,-4.12542049899519,339.24424204261));
#10237=CARTESIAN_POINT('Ctrl Pts',(153.1897852906,-4.00972475439736,339.350866345508));
#10238=CARTESIAN_POINT('Ctrl Pts',(153.182377209456,-3.89414033166249,339.457388055039));
#10239=CARTESIAN_POINT('Ctrl Pts',(153.174969128312,-3.77419053985757,339.559409135248));
#10240=CARTESIAN_POINT('Ctrl Pts',(153.167561047168,-3.65026337667555,339.656555362433));
#10241=CARTESIAN_POINT('Ctrl Pts',(153.160158479993,-3.52642845474449,339.753629281907));
#10242=CARTESIAN_POINT('Ctrl Pts',(153.152755912819,-3.3986223485477,339.845835343851));
#10243=CARTESIAN_POINT('Ctrl Pts',(153.145353345645,-3.26726782940339,339.932838076954));
#10244=CARTESIAN_POINT('Ctrl Pts',(153.137954675891,-3.13598246783996,340.019795003497));
#10245=CARTESIAN_POINT('Ctrl Pts',(153.130556006136,-3.00115272437315,340.101553851564));
#10246=CARTESIAN_POINT('Ctrl Pts',(153.123157336381,-2.86323208885197,340.177821218222));
#10247=CARTESIAN_POINT('Ctrl Pts',(153.115759887177,-2.7253342059523,340.254076003133));
#10248=CARTESIAN_POINT('Ctrl Pts',(153.108362437973,-2.58434676927163,340.324840924172));
#10249=CARTESIAN_POINT('Ctrl Pts',(153.100964988769,-2.44074982231113,340.389867425771));
#10250=CARTESIAN_POINT('Ctrl Pts',(153.093567860306,-2.29715910146383,340.454891107934));
#10251=CARTESIAN_POINT('Ctrl Pts',(153.086170731842,-2.15095943528097,340.514176711413));
#10252=CARTESIAN_POINT('Ctrl Pts',(153.078773603379,-2.00265265036829,340.567523051095));
#10253=CARTESIAN_POINT('Ctrl Pts',(153.071375335942,-1.8543230299127,340.620877604782));
#10254=CARTESIAN_POINT('Ctrl Pts',(153.063977068506,-1.70388599592165,340.668290947457));
#10255=CARTESIAN_POINT('Ctrl Pts',(153.056578801069,-1.55186025930991,340.709611221272));
#10256=CARTESIAN_POINT('Ctrl Pts',(153.049177934543,-1.3997811144589,340.750946011333));
#10257=CARTESIAN_POINT('Ctrl Pts',(153.041777068017,-1.24611251567413,340.78618337286));
#10258=CARTESIAN_POINT('Ctrl Pts',(153.034376201492,-1.09138498298361,340.815222212557));
#10259=CARTESIAN_POINT('Ctrl Pts',(153.026967208107,-0.936487544669095,
340.844292939676));
#10260=CARTESIAN_POINT('Ctrl Pts',(153.019558214722,-0.780529217279805,
340.867151483));
#10261=CARTESIAN_POINT('Ctrl Pts',(153.012149221337,-0.624048020166595,
340.883748348717));
#10262=CARTESIAN_POINT('Ctrl Pts',(153.004735663757,-0.467470425238686,
340.900355438675));
#10263=CARTESIAN_POINT('Ctrl Pts',(152.997322106177,-0.310369690284292,
340.910693140179));
#10264=CARTESIAN_POINT('Ctrl Pts',(152.989908548597,-0.15328497797278,340.914764093185));
#10265=CARTESIAN_POINT('Ctrl Pts',(152.98248443646,0.00402337318518967,
340.918840841938));
#10266=CARTESIAN_POINT('Ctrl Pts',(152.975060324323,0.161315283973783,340.916633028671));
#10267=CARTESIAN_POINT('Ctrl Pts',(152.967636212186,0.31805474642866,340.908195303202));
#10268=CARTESIAN_POINT('Ctrl Pts',(152.963779087032,0.399487207609809,340.903811565112));
#10269=CARTESIAN_POINT('Ctrl Pts',(152.959921961877,0.480770675051538,340.897747086226));
#10270=CARTESIAN_POINT('Ctrl Pts',(152.956064836722,0.561831066392708,340.890014975816));
#10271=CARTESIAN_POINT('Ctrl Pts',(152.948640859284,0.717851545969991,340.875132644824));
#10272=CARTESIAN_POINT('Ctrl Pts',(152.941216881846,0.873515655144116,340.854024347346));
#10273=CARTESIAN_POINT('Ctrl Pts',(152.933792904408,1.02828664465397,340.826710662022));
#10274=CARTESIAN_POINT('Ctrl Pts',(152.926377688381,1.18287498110973,340.799429210957));
#10275=CARTESIAN_POINT('Ctrl Pts',(152.918962472353,1.33657193197829,340.765957013405));
#10276=CARTESIAN_POINT('Ctrl Pts',(152.911547256325,1.48884418903739,340.726366521912));
#10277=CARTESIAN_POINT('Ctrl Pts',(152.904139175181,1.64096993049717,340.68681412419));
#10278=CARTESIAN_POINT('Ctrl Pts',(152.896731094037,1.7916733484325,340.641155245714));
#10279=CARTESIAN_POINT('Ctrl Pts',(152.889323012893,1.94042978233305,340.589513648103));
#10280=CARTESIAN_POINT('Ctrl Pts',(152.881920445719,2.08907549410281,340.537910488277));
#10281=CARTESIAN_POINT('Ctrl Pts',(152.874517878545,2.23577675629784,340.480333597854));
#10282=CARTESIAN_POINT('Ctrl Pts',(152.867115311371,2.38002267811506,340.416956951477));
#10283=CARTESIAN_POINT('Ctrl Pts',(152.859716641616,2.52419265508479,340.353613672628));
#10284=CARTESIAN_POINT('Ctrl Pts',(152.852317971862,2.66590952539194,340.284476868891));
#10285=CARTESIAN_POINT('Ctrl Pts',(152.844919302107,2.80468115087269,340.209769112393));
#10286=CARTESIAN_POINT('Ctrl Pts',(152.837521852903,2.94342988334475,340.135073680354));
#10287=CARTESIAN_POINT('Ctrl Pts',(152.830124403699,3.0792340069957,340.054809296279));
#10288=CARTESIAN_POINT('Ctrl Pts',(152.822726954495,3.211624727061,339.969245131308));
#10289=CARTESIAN_POINT('Ctrl Pts',(152.815329826032,3.3440097068956,339.88368467625));
#10290=CARTESIAN_POINT('Ctrl Pts',(152.807932697568,3.4729812639703,339.792825099774));
#10291=CARTESIAN_POINT('Ctrl Pts',(152.800535569105,3.59809865026128,339.696979525768));
#10292=CARTESIAN_POINT('Ctrl Pts',(152.793137301668,3.72323530150648,339.601119193937));
#10293=CARTESIAN_POINT('Ctrl Pts',(152.785739034231,3.84451630404892,339.50027156292));
#10294=CARTESIAN_POINT('Ctrl Pts',(152.778340766795,3.96153325314481,339.394790648794));
#10295=CARTESIAN_POINT('Ctrl Pts',(152.770939900269,4.07859131152499,339.289272678115));
#10296=CARTESIAN_POINT('Ctrl Pts',(152.763539033743,4.19138205689374,339.179118433262));
#10297=CARTESIAN_POINT('Ctrl Pts',(152.756138167218,4.29953338291418,339.064719332464));
#10298=CARTESIAN_POINT('Ctrl Pts',(152.748729173833,4.40780346943071,338.950194610516));
#10299=CARTESIAN_POINT('Ctrl Pts',(152.741320180448,4.51142370601488,338.831415995204));
#10300=CARTESIAN_POINT('Ctrl Pts',(152.733911187063,4.61006131912147,338.708809134539));
#10301=CARTESIAN_POINT('Ctrl Pts',(152.726497629483,4.70875969640019,338.586126743818));
#10302=CARTESIAN_POINT('Ctrl Pts',(152.719084071903,4.80246911226237,338.459611707658));
#10303=CARTESIAN_POINT('Ctrl Pts',(152.711670514323,4.89090001484624,338.329718848083));
#10304=CARTESIAN_POINT('Ctrl Pts',(152.704246402186,4.97945681500932,338.199641062241));
#10305=CARTESIAN_POINT('Ctrl Pts',(152.696822290049,5.06271989606705,338.06617616434));
#10306=CARTESIAN_POINT('Ctrl Pts',(152.689398177913,5.1404451495519,337.929804469064));
#10307=CARTESIAN_POINT('Ctrl Pts',(152.685541052758,5.18082654800784,337.858953882953));
#10308=CARTESIAN_POINT('Ctrl Pts',(152.681683927603,5.21971394660945,337.78731904357));
#10309=CARTESIAN_POINT('Ctrl Pts',(152.677826802448,5.25707827900714,337.714969342532));
#10310=CARTESIAN_POINT('Ctrl Pts',(152.67040282501,5.32899504332747,337.575714709457));
#10311=CARTESIAN_POINT('Ctrl Pts',(152.662978847572,5.39548340713141,337.433390528146));
#10312=CARTESIAN_POINT('Ctrl Pts',(152.655554870134,5.45627020961228,337.288459298785));
#10313=CARTESIAN_POINT('Ctrl Pts',(152.648139654107,5.51698527452039,337.143699110082));
#10314=CARTESIAN_POINT('Ctrl Pts',(152.640724438079,5.57201202874473,336.996338338386));
#10315=CARTESIAN_POINT('Ctrl Pts',(152.633309222052,5.62112279549672,336.84686466219));
#10316=CARTESIAN_POINT('Ctrl Pts',(152.625901140908,5.67018630811622,336.697534808813));
#10317=CARTESIAN_POINT('Ctrl Pts',(152.618493059763,5.7133450499217,336.546096450506));
#10318=CARTESIAN_POINT('Ctrl Pts',(152.611084978619,5.7504191707918,336.393057759998));
#10319=CARTESIAN_POINT('Ctrl Pts',(152.603682411445,5.78746569671659,336.240132978983));
#10320=CARTESIAN_POINT('Ctrl Pts',(152.596279844271,5.81843653190088,336.085610598699));
#10321=CARTESIAN_POINT('Ctrl Pts',(152.588877277097,5.843201503006,335.930014385786));
#10322=CARTESIAN_POINT('Ctrl Pts',(152.581478607343,5.86795343546202,335.774500093599));
#10323=CARTESIAN_POINT('Ctrl Pts',(152.574079937588,5.88650595246598,335.617913462389));
#10324=CARTESIAN_POINT('Ctrl Pts',(152.566681267833,5.89877989546819,335.460788788189));
#10325=CARTESIAN_POINT('Ctrl Pts',(152.559283818629,5.91105181365097,335.303690034679));
#10326=CARTESIAN_POINT('Ctrl Pts',(152.551886369425,5.91704718446333,335.146053786055));
#10327=CARTESIAN_POINT('Ctrl Pts',(152.544488920221,5.91673866791336,334.988419925784));
#10328=CARTESIAN_POINT('Ctrl Pts',(152.537091791758,5.91643016474013,334.830792900242));
#10329=CARTESIAN_POINT('Ctrl Pts',(152.529694663294,5.90981831839625,334.673168636057));
#10330=CARTESIAN_POINT('Ctrl Pts',(152.522297534831,5.89692792739588,334.516087216951));
#10331=CARTESIAN_POINT('Ctrl Pts',(152.514899267394,5.88403555159709,334.358981611227));
#10332=CARTESIAN_POINT('Ctrl Pts',(152.507500999958,5.86486273676256,334.202419388993));
#10333=CARTESIAN_POINT('Ctrl Pts',(152.500102732521,5.83948617132484,334.046935564924));
#10334=CARTESIAN_POINT('Ctrl Pts',(152.492701865995,5.81410069083268,333.891397117753));
#10335=CARTESIAN_POINT('Ctrl Pts',(152.485300999469,5.78250718054896,333.736938191147));
#10336=CARTESIAN_POINT('Ctrl Pts',(152.477900132944,5.74483342432099,333.584083516127));
#10337=CARTESIAN_POINT('Ctrl Pts',(152.470491139559,5.70711829870718,333.431060992061));
#10338=CARTESIAN_POINT('Ctrl Pts',(152.463082146174,5.66330968280516,333.279646600216));
#10339=CARTESIAN_POINT('Ctrl Pts',(152.455673152789,5.61358543024608,333.130350519528));
#10340=CARTESIAN_POINT('Ctrl Pts',(152.448259595209,5.56383054583228,332.980962467304));
#10341=CARTESIAN_POINT('Ctrl Pts',(152.440846037629,5.50815289481398,332.833695674806));
#10342=CARTESIAN_POINT('Ctrl Pts',(152.433432480049,5.44677825360676,332.689039762666));
#10343=CARTESIAN_POINT('Ctrl Pts',(152.426008367912,5.38531623436161,332.544177906353));
#10344=CARTESIAN_POINT('Ctrl Pts',(152.418584255775,5.31814118516296,332.401934690683));
#10345=CARTESIAN_POINT('Ctrl Pts',(152.411160143639,5.24552491177776,332.262775317512));
#10346=CARTESIAN_POINT('Ctrl Pts',(152.407303018484,5.20779783417411,332.1904764205));
#10347=CARTESIAN_POINT('Ctrl Pts',(152.403445893329,5.16860277221613,332.119009455393));
#10348=CARTESIAN_POINT('Ctrl Pts',(152.399588768174,5.12798234932573,332.04843641649));
#10349=CARTESIAN_POINT('Ctrl Pts',(152.392164790736,5.04979844526201,331.912601402709));
#10350=CARTESIAN_POINT('Ctrl Pts',(152.384740813298,4.96609567359945,331.779670138052));
#10351=CARTESIAN_POINT('Ctrl Pts',(152.37731683586,4.87711513762627,331.650122614656));
#10352=CARTESIAN_POINT('Ctrl Pts',(152.369901619833,4.78823961207352,331.52072797683));
#10353=CARTESIAN_POINT('Ctrl Pts',(152.362486403805,4.69409892949561,331.394709436135));
#10354=CARTESIAN_POINT('Ctrl Pts',(152.355071187777,4.59497998016596,331.272522361653));
#10355=CARTESIAN_POINT('Ctrl Pts',(152.347663106633,4.49595640259028,331.15045285496));
#10356=CARTESIAN_POINT('Ctrl Pts',(152.340255025489,4.39196432793274,331.032207763013));
#10357=CARTESIAN_POINT('Ctrl Pts',(152.332846944345,4.28333376226275,330.918213327039));
#10358=CARTESIAN_POINT('Ctrl Pts',(152.325444377171,4.17478405230648,330.804303739206));
#10359=CARTESIAN_POINT('Ctrl Pts',(152.318041809997,4.06160298215941,330.694638776702));
#10360=CARTESIAN_POINT('Ctrl Pts',(152.310639242823,3.94416055409882,330.589611345245));
#10361=CARTESIAN_POINT('Ctrl Pts',(152.303240573068,3.82677995896376,330.484639210273));
#10362=CARTESIAN_POINT('Ctrl Pts',(152.295841903314,3.70514275164424,330.384299991837));
#10363=CARTESIAN_POINT('Ctrl Pts',(152.288443233559,3.57965539583741,330.288949394291));
#10364=CARTESIAN_POINT('Ctrl Pts',(152.281045784355,3.45418874154727,330.193614526632));
#10365=CARTESIAN_POINT('Ctrl Pts',(152.273648335151,3.32487349621752,330.103266872114));
#10366=CARTESIAN_POINT('Ctrl Pts',(152.266250885947,3.19214886413591,330.018221583441));
#10367=CARTESIAN_POINT('Ctrl Pts',(152.258853757483,3.0594299867632,329.933179982183));
#10368=CARTESIAN_POINT('Ctrl Pts',(152.25145662902,2.9233023307996,329.853440491003));
#10369=CARTESIAN_POINT('Ctrl Pts',(152.244059500556,2.78423348406682,329.779274526591));
#10370=CARTESIAN_POINT('Ctrl Pts',(152.23666123312,2.64514322420307,329.705097142472));
#10371=CARTESIAN_POINT('Ctrl Pts',(152.229262965683,2.50311120117458,329.636495169511));
#10372=CARTESIAN_POINT('Ctrl Pts',(152.221864698246,2.35862882074756,329.57369364591));
#10373=CARTESIAN_POINT('Ctrl Pts',(152.214463831721,2.21409568214128,329.510870059473));
#10374=CARTESIAN_POINT('Ctrl Pts',(152.207062965195,2.06711081427276,329.453851128251));
#10375=CARTESIAN_POINT('Ctrl Pts',(152.199662098669,1.91818462582289,329.402813358145));
#10376=CARTESIAN_POINT('Ctrl Pts',(152.192253105284,1.76909490217986,329.351719543688));
#10377=CARTESIAN_POINT('Ctrl Pts',(152.1848441119,1.61805995399045,329.306620127833));
#10378=CARTESIAN_POINT('Ctrl Pts',(152.177435118515,1.46560504840998,329.267641636763));
#10379=CARTESIAN_POINT('Ctrl Pts',(152.170021560935,1.31305622534886,329.228639133597));
#10380=CARTESIAN_POINT('Ctrl Pts',(152.162608003354,1.15908606598829,329.195765146582));
#10381=CARTESIAN_POINT('Ctrl Pts',(152.155194445774,1.00422848333707,329.16909477733));
#10382=CARTESIAN_POINT('Ctrl Pts',(152.147770333637,0.849150432566782,329.142386437926));
#10383=CARTESIAN_POINT('Ctrl Pts',(152.140346221501,0.693182804258974,329.121899404001));
#10384=CARTESIAN_POINT('Ctrl Pts',(152.132922109364,0.536863886274555,329.107656855705));
#10385=CARTESIAN_POINT('Ctrl Pts',(152.12906498421,0.455649914880493,329.100257278452));
#10386=CARTESIAN_POINT('Ctrl Pts',(152.125207859055,0.374341122206674,329.094542366649));
#10387=CARTESIAN_POINT('Ctrl Pts',(152.1213507339,0.293012706561376,329.090509826026));
#10388=CARTESIAN_POINT('Ctrl Pts',(152.113926756462,0.136476348880449,329.082748218766));
#10389=CARTESIAN_POINT('Ctrl Pts',(152.106502779024,-0.0206047601445989,
329.081198930277));
#10390=CARTESIAN_POINT('Ctrl Pts',(152.099078801586,-0.177696510059613,
329.085918962948));
#10391=CARTESIAN_POINT('Ctrl Pts',(152.091663585559,-0.334602868073692,
329.090633425272));
#10392=CARTESIAN_POINT('Ctrl Pts',(152.084248369531,-0.491519472565919,
329.101602470342));
#10393=CARTESIAN_POINT('Ctrl Pts',(152.076833153504,-0.647908141170273,
329.118831272349));
#10394=CARTESIAN_POINT('Ctrl Pts',(152.069425072359,-0.804146333385481,
329.136043496889));
#10395=CARTESIAN_POINT('Ctrl Pts',(152.062016991215,-0.959857232513241,
329.159503446887));
#10396=CARTESIAN_POINT('Ctrl Pts',(152.054608910071,-1.11450381799239,329.189164276786));
#10397=CARTESIAN_POINT('Ctrl Pts',(152.047206342897,-1.26903529719323,329.218803029587));
#10398=CARTESIAN_POINT('Ctrl Pts',(152.039803775723,-1.42250367514679,329.254633402301));
#10399=CARTESIAN_POINT('Ctrl Pts',(152.032401208549,-1.57437831958847,329.296556875947));
#10400=CARTESIAN_POINT('Ctrl Pts',(152.025002538794,-1.72617300269303,329.338458277067));
#10401=CARTESIAN_POINT('Ctrl Pts',(152.01760386904,-1.87637526454022,329.386446291159));
#10402=CARTESIAN_POINT('Ctrl Pts',(152.010205199285,-2.02446602492158,329.440371606264));
#10403=CARTESIAN_POINT('Ctrl Pts',(152.002807750081,-2.17253235492683,329.494288025366));
#10404=CARTESIAN_POINT('Ctrl Pts',(151.995410300877,-2.31848752444893,329.554139673976));
#10405=CARTESIAN_POINT('Ctrl Pts',(151.988012851673,-2.46182883621265,329.61972776305));
#10406=CARTESIAN_POINT('Ctrl Pts',(151.98061572321,-2.6051639329473,329.685313008339));
#10407=CARTESIAN_POINT('Ctrl Pts',(151.973218594746,-2.7458850578937,329.756634044267));
#10408=CARTESIAN_POINT('Ctrl Pts',(151.965821466283,-2.88351093236498,329.833444545402));
#10409=CARTESIAN_POINT('Ctrl Pts',(151.958423198846,-3.0211579977855,329.910266873438));
#10410=CARTESIAN_POINT('Ctrl Pts',(151.951024931409,-3.15570853786383,329.992580167774));
#10411=CARTESIAN_POINT('Ctrl Pts',(151.943626663973,-3.28670738531855,330.0800929759));
#10412=CARTESIAN_POINT('Ctrl Pts',(151.936225797447,-3.41775225404523,330.167636528195));
#10413=CARTESIAN_POINT('Ctrl Pts',(151.928824930921,-3.54524263574842,330.26038302394));
#10414=CARTESIAN_POINT('Ctrl Pts',(151.921424064396,-3.66875389142648,330.357998767057));
#10415=CARTESIAN_POINT('Ctrl Pts',(151.914015071011,-3.79240077427206,330.455721701593));
#10416=CARTESIAN_POINT('Ctrl Pts',(151.906606077626,-3.91205951206739,330.558324329992));
#10417=CARTESIAN_POINT('Ctrl Pts',(151.899197084241,-4.0273394540485,330.665433414473));
#10418=CARTESIAN_POINT('Ctrl Pts',(151.891783526661,-4.14269041244969,330.772608481845));
#10419=CARTESIAN_POINT('Ctrl Pts',(151.884369969081,-4.25365693750218,330.884295272977));
#10420=CARTESIAN_POINT('Ctrl Pts',(151.876956411501,-4.35988694369155,331.000085450822));
#10421=CARTESIAN_POINT('Ctrl Pts',(151.869532299364,-4.46626818774307,331.116040477183));
#10422=CARTESIAN_POINT('Ctrl Pts',(151.862108187227,-4.56789920474008,331.236110273648));
#10423=CARTESIAN_POINT('Ctrl Pts',(151.854684075091,-4.66446920355254,331.359854726579));
#10424=CARTESIAN_POINT('Ctrl Pts',(151.850826949936,-4.7146412059084,331.424144951911));
#10425=CARTESIAN_POINT('Ctrl Pts',(151.846969824781,-4.76344785038058,331.489426583622));
#10426=CARTESIAN_POINT('Ctrl Pts',(151.843112699626,-4.81085037215204,331.555635144288));
#10427=CARTESIAN_POINT('Ctrl Pts',(151.83562238215,-4.90290337095759,331.684208400059));
#10428=CARTESIAN_POINT('Ctrl Pts',(151.828132064673,-4.98993472057112,331.816664597315));
#10429=CARTESIAN_POINT('Ctrl Pts',(151.820641747196,-5.07160260010362,331.952578527817));
#10430=CARTESIAN_POINT('Ctrl Pts',(151.813160572798,-5.15317079149597,332.088326554576));
#10431=CARTESIAN_POINT('Ctrl Pts',(151.8056793984,-5.22938835994049,332.227523603511));
#10432=CARTESIAN_POINT('Ctrl Pts',(151.798198224001,-5.29995476856217,332.369712940819));
#10433=CARTESIAN_POINT('Ctrl Pts',(151.790724794843,-5.37044811997292,332.511755069893));
#10434=CARTESIAN_POINT('Ctrl Pts',(151.783251365684,-5.43530179937797,332.656782995412));
#10435=CARTESIAN_POINT('Ctrl Pts',(151.775777936525,-5.49425952383021,332.80431267087));
#10436=CARTESIAN_POINT('Ctrl Pts',(151.768310859863,-5.55316713357213,332.951716944492));
#10437=CARTESIAN_POINT('Ctrl Pts',(151.7608437832,-5.60618863382233,333.101618396629));
#10438=CARTESIAN_POINT('Ctrl Pts',(151.753376706538,-5.65311452289628,333.253510162206));
#10439=CARTESIAN_POINT('Ctrl Pts',(151.745915097621,-5.70000605062241,333.405290705472));
#10440=CARTESIAN_POINT('Ctrl Pts',(151.738453488704,-5.74081075387373,333.55905831107));
#10441=CARTESIAN_POINT('Ctrl Pts',(151.730991879787,-5.77536800135642,333.714288130486));
#10442=CARTESIAN_POINT('Ctrl Pts',(151.723533523754,-5.80991018362923,333.869450277563));
#10443=CARTESIAN_POINT('Ctrl Pts',(151.716075167721,-5.8382102557323,334.026073013779));
#10444=CARTESIAN_POINT('Ctrl Pts',(151.708616811688,-5.86015796662616,334.18361824574));
#10445=CARTESIAN_POINT('Ctrl Pts',(151.70115959323,-5.88210232997663,334.341139448339));
#10446=CARTESIAN_POINT('Ctrl Pts',(151.693702374772,-5.89769620725362,334.499582506367));
#10447=CARTESIAN_POINT('Ctrl Pts',(151.686245156313,-5.90688078937849,334.65840096228));
#10448=CARTESIAN_POINT('Ctrl Pts',(151.68084743911,-5.91352881467381,334.773357647071));
#10449=CARTESIAN_POINT('Ctrl Pts',(151.675449721906,-5.91681994241088,334.888510813414));
#10450=CARTESIAN_POINT('Ctrl Pts',(151.670052004703,-5.9167488729118,335.003652040113));
#10451=CARTESIAN_POINT('',(149.920053353871,-5.92109797199052,335.003013532025));
#10452=CARTESIAN_POINT('Ctrl Pts',(151.670049900736,-5.90929938065838,335.003692266209));
#10453=CARTESIAN_POINT('Ctrl Pts',(151.634991488942,-5.9134882699069,335.750600828835));
#10454=CARTESIAN_POINT('Ctrl Pts',(151.507187065722,-5.43515578827606,338.468256395567));
#10455=CARTESIAN_POINT('Ctrl Pts',(151.286636631079,-1.35011516578284,341.865115582446));
#10456=CARTESIAN_POINT('Ctrl Pts',(151.008398596804,5.04239736829986,339.850448608261));
#10457=CARTESIAN_POINT('Ctrl Pts',(150.73016056253,6.80757626315719,333.384596538777));
#10458=CARTESIAN_POINT('Ctrl Pts',(150.451922528256,2.32554290097631,328.401176382346));
#10459=CARTESIAN_POINT('Ctrl Pts',(150.181887150958,-4.095558012434,329.44178936122));
#10460=CARTESIAN_POINT('Ctrl Pts',(150.004597785083,-5.91334784080282,333.213692926844));
#10461=CARTESIAN_POINT('Ctrl Pts',(149.920054430632,-5.92456868112744,335.002992526362));
#10462=CARTESIAN_POINT('',(148.170052004658,-5.91674764560021,334.994721668406));
#10463=CARTESIAN_POINT('Ctrl Pts',(149.920052004703,-5.91674921910679,335.003039851844));
#10464=CARTESIAN_POINT('Ctrl Pts',(149.911850156372,-5.91666015362462,335.176396366927));
#10465=CARTESIAN_POINT('Ctrl Pts',(149.90364830804,-5.9089529647869,335.349551836332));
#10466=CARTESIAN_POINT('Ctrl Pts',(149.895446459709,-5.89367613405626,335.5220270006));
#10467=CARTESIAN_POINT('Ctrl Pts',(149.888022482271,-5.87984817210363,335.678144460519));
#10468=CARTESIAN_POINT('Ctrl Pts',(149.880598504833,-5.85979197820686,335.833947619004));
#10469=CARTESIAN_POINT('Ctrl Pts',(149.873174527395,-5.83352450441269,335.988899600018));
#10470=CARTESIAN_POINT('Ctrl Pts',(149.865759311367,-5.80728803018976,336.143668714382));
#10471=CARTESIAN_POINT('Ctrl Pts',(149.858344095339,-5.77485492880872,336.297588286399));
#10472=CARTESIAN_POINT('Ctrl Pts',(149.850928879312,-5.73629404828548,336.450124530551));
#10473=CARTESIAN_POINT('Ctrl Pts',(149.843520798168,-5.69777027084729,336.602514005096));
#10474=CARTESIAN_POINT('Ctrl Pts',(149.836112717024,-5.65313054319746,336.7535224422));
#10475=CARTESIAN_POINT('Ctrl Pts',(149.82870463588,-5.6024950796755,336.902624357227));
#10476=CARTESIAN_POINT('Ctrl Pts',(149.821302068706,-5.55189730505386,337.051615292975));
#10477=CARTESIAN_POINT('Ctrl Pts',(149.813899501532,-5.49531280001478,337.198702180324));
#10478=CARTESIAN_POINT('Ctrl Pts',(149.806496934358,-5.43291208380104,337.343372964807));
#10479=CARTESIAN_POINT('Ctrl Pts',(149.799098264603,-5.37054422129158,337.487967580755));
#10480=CARTESIAN_POINT('Ctrl Pts',(149.791699594848,-5.30236639362072,337.630148285406));
#10481=CARTESIAN_POINT('Ctrl Pts',(149.784300925093,-5.2285978430923,337.769421448193));
#10482=CARTESIAN_POINT('Ctrl Pts',(149.776903475889,-5.15484146208413,337.908671635233));
#10483=CARTESIAN_POINT('Ctrl Pts',(149.769506026685,-5.0754963631945,338.045014902884));
#10484=CARTESIAN_POINT('Ctrl Pts',(149.762108577482,-4.99082854437905,338.177980648637));
#10485=CARTESIAN_POINT('Ctrl Pts',(149.754711449018,-4.90616439661264,338.310940629227));
#10486=CARTESIAN_POINT('Ctrl Pts',(149.747314320555,-4.8161781882525,338.44052306429));
#10487=CARTESIAN_POINT('Ctrl Pts',(149.739917192091,-4.72118005847716,338.566285100484));
#10488=CARTESIAN_POINT('Ctrl Pts',(149.732518924655,-4.62616730136124,338.692066500893));
#10489=CARTESIAN_POINT('Ctrl Pts',(149.725120657218,-4.52614131121688,338.814026033343));
#10490=CARTESIAN_POINT('Ctrl Pts',(149.717722389781,-4.42145333697985,338.931752910778));
#10491=CARTESIAN_POINT('Ctrl Pts',(149.710321523256,-4.31672858475645,339.049521146903));
#10492=CARTESIAN_POINT('Ctrl Pts',(149.70292065673,-4.20733883542256,339.16305348873));
#10493=CARTESIAN_POINT('Ctrl Pts',(149.695519790204,-4.09367298442977,339.271975194105));
#10494=CARTESIAN_POINT('Ctrl Pts',(149.68811079682,-3.97988231746572,339.381016505926));
#10495=CARTESIAN_POINT('Ctrl Pts',(149.680701803435,-3.86180644116627,339.485436812003));
#10496=CARTESIAN_POINT('Ctrl Pts',(149.67329281005,-3.73986874570421,339.584900470829));
#10497=CARTESIAN_POINT('Ctrl Pts',(149.66587925247,-3.61785593241605,339.684425402699));
#10498=CARTESIAN_POINT('Ctrl Pts',(149.65846569489,-3.49197685716381,339.77898737925));
#10499=CARTESIAN_POINT('Ctrl Pts',(149.651052137309,-3.36268437546262,339.868293782581));
#10500=CARTESIAN_POINT('Ctrl Pts',(149.643628025173,-3.23320782224322,339.957727329927));
#10501=CARTESIAN_POINT('Ctrl Pts',(149.636203913036,-3.10030847141647,340.041890161325));
#10502=CARTESIAN_POINT('Ctrl Pts',(149.628779800899,-2.96446497757998,340.120534929009));
#10503=CARTESIAN_POINT('Ctrl Pts',(149.624922675745,-2.89388881338412,340.161394052111));
#10504=CARTESIAN_POINT('Ctrl Pts',(149.62106555059,-2.82251832078065,340.20076450764));
#10505=CARTESIAN_POINT('Ctrl Pts',(149.617208425435,-2.75042269343963,340.238616761122));
#10506=CARTESIAN_POINT('Ctrl Pts',(149.609784447997,-2.61165708711303,340.31147264849));
#10507=CARTESIAN_POINT('Ctrl Pts',(149.60236047056,-2.46978532988706,340.378920996201));
#10508=CARTESIAN_POINT('Ctrl Pts',(149.594936493122,-2.32526806599919,340.440685525165));
#10509=CARTESIAN_POINT('Ctrl Pts',(149.587521277094,-2.18092135422653,340.502377162692));
#10510=CARTESIAN_POINT('Ctrl Pts',(149.580106061066,-2.03393569021874,340.558398188133));
#10511=CARTESIAN_POINT('Ctrl Pts',(149.572690845039,-1.88479720321985,340.608517635279));
#10512=CARTESIAN_POINT('Ctrl Pts',(149.565282763895,-1.73580221652222,340.658588857745));
#10513=CARTESIAN_POINT('Ctrl Pts',(149.55787468275,-1.5846588820798,340.702769688597));
#10514=CARTESIAN_POINT('Ctrl Pts',(149.550466601606,-1.43187414601021,340.740876848748));
#10515=CARTESIAN_POINT('Ctrl Pts',(149.543064034432,-1.27920313041009,340.778955645044));
#10516=CARTESIAN_POINT('Ctrl Pts',(149.535661467258,-1.12489350638225,340.810969682167));
#10517=CARTESIAN_POINT('Ctrl Pts',(149.528258900084,-0.969468149198965,
340.836785251334));
#10518=CARTESIAN_POINT('Ctrl Pts',(149.52086023033,-0.814124622786566,340.862587228716));
#10519=CARTESIAN_POINT('Ctrl Pts',(149.513461560575,-0.657666900357778,
340.882197176531));
#10520=CARTESIAN_POINT('Ctrl Pts',(149.50606289082,-0.500628730977748,340.895532328486));
#10521=CARTESIAN_POINT('Ctrl Pts',(149.498665441616,-0.343616468019706,
340.908865280554));
#10522=CARTESIAN_POINT('Ctrl Pts',(149.491267992412,-0.186024319665954,
340.915925459645));
#10523=CARTESIAN_POINT('Ctrl Pts',(149.483870543208,-0.0283919723632106,
340.916681879094));
#10524=CARTESIAN_POINT('Ctrl Pts',(149.476473414745,0.129233540275767,340.917438265747));
#10525=CARTESIAN_POINT('Ctrl Pts',(149.469076286281,0.286898875191166,340.911891434416));
#10526=CARTESIAN_POINT('Ctrl Pts',(149.461679157818,0.444063793455606,340.900062534401));
#10527=CARTESIAN_POINT('Ctrl Pts',(149.454280890381,0.601252911194095,340.88823181303));
#10528=CARTESIAN_POINT('Ctrl Pts',(149.446882622944,0.757941086680273,340.870117125002));
#10529=CARTESIAN_POINT('Ctrl Pts',(149.439484355508,0.913592799362333,340.845791542593));
#10530=CARTESIAN_POINT('Ctrl Pts',(149.432083488982,1.06929919412793,340.821457414351));
#10531=CARTESIAN_POINT('Ctrl Pts',(149.424682622456,1.22396803262342,340.790908105056));
#10532=CARTESIAN_POINT('Ctrl Pts',(149.41728175593,1.3770737325329,340.754267850706));
#10533=CARTESIAN_POINT('Ctrl Pts',(149.409872762546,1.53034755713853,340.717587361854));
#10534=CARTESIAN_POINT('Ctrl Pts',(149.402463769161,1.6820544520858,340.67480265769));
#10535=CARTESIAN_POINT('Ctrl Pts',(149.395054775776,1.83168304855458,340.626088141163));
#10536=CARTESIAN_POINT('Ctrl Pts',(149.387641218196,1.98140382139997,340.577343614815));
#10537=CARTESIAN_POINT('Ctrl Pts',(149.380227660616,2.12904339543219,340.522662126399));
#10538=CARTESIAN_POINT('Ctrl Pts',(149.372814103035,2.27411063591168,340.462266139446));
#10539=CARTESIAN_POINT('Ctrl Pts',(149.365389990899,2.41938440616606,340.401784167747));
#10540=CARTESIAN_POINT('Ctrl Pts',(149.357965878762,2.56207819111879,340.335571605685));
#10541=CARTESIAN_POINT('Ctrl Pts',(149.350541766625,2.70172496328973,340.263897110054));
#10542=CARTESIAN_POINT('Ctrl Pts',(149.346684641471,2.77427708370367,340.226659323911));
#10543=CARTESIAN_POINT('Ctrl Pts',(149.342827516316,2.84600720847702,340.187947966621));
#10544=CARTESIAN_POINT('Ctrl Pts',(149.338970391161,2.91685305677357,340.147805241818));
#10545=CARTESIAN_POINT('Ctrl Pts',(149.331546413723,3.05321315872498,340.070540784148));
#10546=CARTESIAN_POINT('Ctrl Pts',(149.324122436285,3.18670686169737,339.987737967928));
#10547=CARTESIAN_POINT('Ctrl Pts',(149.316698458847,3.31685255568017,339.899634648255));
#10548=CARTESIAN_POINT('Ctrl Pts',(149.30928324282,3.44684465816264,339.811635303754));
#10549=CARTESIAN_POINT('Ctrl Pts',(149.301868026792,3.57349631044197,339.71834811444));
#10550=CARTESIAN_POINT('Ctrl Pts',(149.294452810764,3.69635021567802,339.620056887697));
#10551=CARTESIAN_POINT('Ctrl Pts',(149.28704472962,3.81908591150498,339.521860236277));
#10552=CARTESIAN_POINT('Ctrl Pts',(149.279636648476,3.93803084559408,339.418669364512));
#10553=CARTESIAN_POINT('Ctrl Pts',(149.272228567332,4.0527565570192,339.310811391378));
#10554=CARTESIAN_POINT('Ctrl Pts',(149.264826000158,4.167396876002,339.203033698904));
#10555=CARTESIAN_POINT('Ctrl Pts',(149.257423432984,4.2778239546545,339.09059607646));
#10556=CARTESIAN_POINT('Ctrl Pts',(149.25002086581,4.38364239659471,338.973865863523));
#10557=CARTESIAN_POINT('Ctrl Pts',(149.242622196055,4.48940512558775,338.857197108534));
#10558=CARTESIAN_POINT('Ctrl Pts',(149.235223526301,4.59056380021348,338.736240539846));
#10559=CARTESIAN_POINT('Ctrl Pts',(149.227824856546,4.68675997828438,338.611400208846));
#10560=CARTESIAN_POINT('Ctrl Pts',(149.220427407342,4.78294028697303,338.486580472624));
#10561=CARTESIAN_POINT('Ctrl Pts',(149.213029958138,4.87415949630309,338.357878541011));
#10562=CARTESIAN_POINT('Ctrl Pts',(149.205632508934,4.96009949362319,338.225731479193));
#10563=CARTESIAN_POINT('Ctrl Pts',(149.198235380471,5.04603576473476,338.093590147042));
#10564=CARTESIAN_POINT('Ctrl Pts',(149.190838252007,5.12669307549016,337.958004294559));
#10565=CARTESIAN_POINT('Ctrl Pts',(149.183441123544,5.20179685650292,337.819439665284));
#10566=CARTESIAN_POINT('Ctrl Pts',(149.176042856107,5.27691220162313,337.680853700515));
#10567=CARTESIAN_POINT('Ctrl Pts',(149.168644588671,5.34647213652136,337.53928837384));
#10568=CARTESIAN_POINT('Ctrl Pts',(149.161246321234,5.41024830833589,337.39523355952));
#10569=CARTESIAN_POINT('Ctrl Pts',(149.153845454708,5.47404688539028,337.251128137227));
#10570=CARTESIAN_POINT('Ctrl Pts',(149.146444588182,5.53205750286878,337.104531827043));
#10571=CARTESIAN_POINT('Ctrl Pts',(149.139043721657,5.58410021072489,336.955953833576));
#10572=CARTESIAN_POINT('Ctrl Pts',(149.131634728272,5.63620006644974,336.807212687268));
#10573=CARTESIAN_POINT('Ctrl Pts',(149.124225734887,5.68231880174213,336.656485864374));
#10574=CARTESIAN_POINT('Ctrl Pts',(149.116816741502,5.72232634475302,336.504297765286));
#10575=CARTESIAN_POINT('Ctrl Pts',(149.109403183922,5.76235853379041,336.352015913081));
#10576=CARTESIAN_POINT('Ctrl Pts',(149.101989626342,5.79627194866979,336.19827135452));
#10577=CARTESIAN_POINT('Ctrl Pts',(149.094576068762,5.8239878825285,336.043597483066));
#10578=CARTESIAN_POINT('Ctrl Pts',(149.087151956625,5.85174327509312,335.888703405038));
#10579=CARTESIAN_POINT('Ctrl Pts',(149.079727844488,5.87328351387791,335.732877740426));
#10580=CARTESIAN_POINT('Ctrl Pts',(149.072303732352,5.88858178274542,335.576658608207));
#10581=CARTESIAN_POINT('Ctrl Pts',(149.068446607197,5.89652984934074,335.495496479531));
#10582=CARTESIAN_POINT('Ctrl Pts',(149.064589482042,5.9027939295139,335.414228150625));
#10583=CARTESIAN_POINT('Ctrl Pts',(149.060732356887,5.90737580946663,335.332928833579));
#10584=CARTESIAN_POINT('Ctrl Pts',(149.053308379449,5.91619475415412,335.176448483254));
#10585=CARTESIAN_POINT('Ctrl Pts',(149.045884402011,5.91880520201925,335.019381425379));
#10586=CARTESIAN_POINT('Ctrl Pts',(149.038460424573,5.91514654367648,334.862261373129));
#10587=CARTESIAN_POINT('Ctrl Pts',(149.031045208546,5.91149220310102,334.705326746181));
#10588=CARTESIAN_POINT('Ctrl Pts',(149.023629992518,5.90158349173057,334.548339618829));
#10589=CARTESIAN_POINT('Ctrl Pts',(149.01621477649,5.88541159968937,334.391838126202));
#10590=CARTESIAN_POINT('Ctrl Pts',(149.008806695346,5.86925526816128,334.235487218523));
#10591=CARTESIAN_POINT('Ctrl Pts',(149.001398614202,5.84684779150791,334.079621384065));
#10592=CARTESIAN_POINT('Ctrl Pts',(148.993990533058,5.8182323862625,333.92477794761));
#10593=CARTESIAN_POINT('Ctrl Pts',(148.986587965884,5.78963827998582,333.770049763952));
#10594=CARTESIAN_POINT('Ctrl Pts',(148.97918539871,5.75484551308457,333.61634282848));
#10595=CARTESIAN_POINT('Ctrl Pts',(148.971782831536,5.71394901749076,333.464188426917));
#10596=CARTESIAN_POINT('Ctrl Pts',(148.964384161781,5.67307405372311,333.31211413398));
#10597=CARTESIAN_POINT('Ctrl Pts',(148.956985492026,5.62610185794155,333.161591106558));
#10598=CARTESIAN_POINT('Ctrl Pts',(148.949586822272,5.5731782319411,333.013139421721));
#10599=CARTESIAN_POINT('Ctrl Pts',(148.942189373068,5.52026333669559,332.864712226803));
#10600=CARTESIAN_POINT('Ctrl Pts',(148.934791923864,5.46139908499283,332.71835604749));
#10601=CARTESIAN_POINT('Ctrl Pts',(148.92739447466,5.39678086526162,332.574574912547));
#10602=CARTESIAN_POINT('Ctrl Pts',(148.919997346196,5.33216544726379,332.430800011704));
#10603=CARTESIAN_POINT('Ctrl Pts',(148.912600217733,5.26179671027868,332.289600273648));
#10604=CARTESIAN_POINT('Ctrl Pts',(148.905203089269,5.18591772273406,332.151458630188));
#10605=CARTESIAN_POINT('Ctrl Pts',(148.897804821833,5.11002705171953,332.013295716363));
#10606=CARTESIAN_POINT('Ctrl Pts',(148.890406554396,5.02862462047629,331.87819216183));
#10607=CARTESIAN_POINT('Ctrl Pts',(148.883008286959,4.94199879988343,331.746605092453));
#10608=CARTESIAN_POINT('Ctrl Pts',(148.875607420434,4.8553425467288,331.614971795155));
#10609=CARTESIAN_POINT('Ctrl Pts',(148.868206553908,4.7634594557651,331.48685775418));
#10610=CARTESIAN_POINT('Ctrl Pts',(148.860805687382,4.66668034671686,331.362689853193));
#10611=CARTESIAN_POINT('Ctrl Pts',(148.853396693997,4.5697949649544,331.238385603979));
#10612=CARTESIAN_POINT('Ctrl Pts',(148.845987700613,4.46800305792502,331.118036443));
#10613=CARTESIAN_POINT('Ctrl Pts',(148.838578707228,4.36167521576677,331.002035533591));
#10614=CARTESIAN_POINT('Ctrl Pts',(148.831165149647,4.25528187199012,330.885963163621));
#10615=CARTESIAN_POINT('Ctrl Pts',(148.823751592067,4.14434728744243,330.77424464704));
#10616=CARTESIAN_POINT('Ctrl Pts',(148.816338034487,4.0292774112641,330.667234819936));
#10617=CARTESIAN_POINT('Ctrl Pts',(148.80891392235,3.91404371205071,330.560072644752));
#10618=CARTESIAN_POINT('Ctrl Pts',(148.801489810214,3.7946632454675,330.45763279002));
#10619=CARTESIAN_POINT('Ctrl Pts',(148.794065698077,3.67157401549325,330.360229013059));
#10620=CARTESIAN_POINT('Ctrl Pts',(148.790208572922,3.60762420487052,330.30962382939));
#10621=CARTESIAN_POINT('Ctrl Pts',(148.786351447768,3.54267378652824,330.260377274791));
#10622=CARTESIAN_POINT('Ctrl Pts',(148.782494322613,3.47678697453515,330.212528548785));
#10623=CARTESIAN_POINT('Ctrl Pts',(148.775070345175,3.34997174658619,330.120432013651));
#10624=CARTESIAN_POINT('Ctrl Pts',(148.767646367737,3.21930336986818,330.033238834829));
#10625=CARTESIAN_POINT('Ctrl Pts',(148.760222390299,3.08519785595913,329.951288802864));
#10626=CARTESIAN_POINT('Ctrl Pts',(148.752807174272,2.95125060673366,329.869435484267));
#10627=CARTESIAN_POINT('Ctrl Pts',(148.745391958244,2.81387460988558,329.792813188522));
#10628=CARTESIAN_POINT('Ctrl Pts',(148.737976742216,2.67351762719648,329.721720539838));
#10629=CARTESIAN_POINT('Ctrl Pts',(148.730568661072,2.53329569528947,329.650696296142));
#10630=CARTESIAN_POINT('Ctrl Pts',(148.723160579928,2.39009881848453,329.585191274698));
#10631=CARTESIAN_POINT('Ctrl Pts',(148.715752498784,2.24440223159955,329.525459911071));
#10632=CARTESIAN_POINT('Ctrl Pts',(148.70834993161,2.09881408934519,329.465773006589));
#10633=CARTESIAN_POINT('Ctrl Pts',(148.700947364436,1.95073028553513,329.411851344062));
#10634=CARTESIAN_POINT('Ctrl Pts',(148.693544797262,1.80064896278255,329.363902602391));
#10635=CARTESIAN_POINT('Ctrl Pts',(148.686146127507,1.6506466571902,329.315979105524));
#10636=CARTESIAN_POINT('Ctrl Pts',(148.678747457753,1.49864928176157,329.274022379917));
#10637=CARTESIAN_POINT('Ctrl Pts',(148.671348787998,1.34517308211892,329.238191261275));
#10638=CARTESIAN_POINT('Ctrl Pts',(148.663951338794,1.19172220128368,329.202366053656));
#10639=CARTESIAN_POINT('Ctrl Pts',(148.65655388959,1.03679334350103,329.172664532185));
#10640=CARTESIAN_POINT('Ctrl Pts',(148.649156440386,0.880916093202752,329.149195149449));
#10641=CARTESIAN_POINT('Ctrl Pts',(148.641759311922,0.725045601470463,329.125726784304));
#10642=CARTESIAN_POINT('Ctrl Pts',(148.634362183459,0.568227168035613,329.108490076185));
#10643=CARTESIAN_POINT('Ctrl Pts',(148.626965054995,0.410998438831725,329.097541965776));
#10644=CARTESIAN_POINT('Ctrl Pts',(148.619566787559,0.253745500328273,329.086592169631));
#10645=CARTESIAN_POINT('Ctrl Pts',(148.612168520122,0.0960825125978685,
329.08193292511));
#10646=CARTESIAN_POINT('Ctrl Pts',(148.604770252686,-0.0614500634389803,
329.083569112023));
#10647=CARTESIAN_POINT('Ctrl Pts',(148.59736938616,-0.219037982326384,329.085205873746));
#10648=CARTESIAN_POINT('Ctrl Pts',(148.589968519634,-0.376495025346606,
329.093142466423));
#10649=CARTESIAN_POINT('Ctrl Pts',(148.582567653108,-0.533283191382411,
329.107331707937));
#10650=CARTESIAN_POINT('Ctrl Pts',(148.575158659724,-0.690243525814229,
329.121536530594));
#10651=CARTESIAN_POINT('Ctrl Pts',(148.567749666339,-0.846533144530133,
329.14200768021));
#10652=CARTESIAN_POINT('Ctrl Pts',(148.560340672954,-1.00162088050476,329.168646282874));
#10653=CARTESIAN_POINT('Ctrl Pts',(148.552927115374,-1.15680415587419,329.195301295836));
#10654=CARTESIAN_POINT('Ctrl Pts',(148.545513557794,-1.31078370900066,329.228131254938));
#10655=CARTESIAN_POINT('Ctrl Pts',(148.538100000213,-1.46304146827509,329.266986811056));
#10656=CARTESIAN_POINT('Ctrl Pts',(148.530675888077,-1.61551599434436,329.305897685171));
#10657=CARTESIAN_POINT('Ctrl Pts',(148.52325177594,-1.7662634741643,329.350851182998));
#10658=CARTESIAN_POINT('Ctrl Pts',(148.515827663803,-1.9147830334263,329.401648769736));
#10659=CARTESIAN_POINT('Ctrl Pts',(148.511970538649,-1.99194492395807,329.42804016119));
#10660=CARTESIAN_POINT('Ctrl Pts',(148.508113413494,-2.06850580057166,329.456008217171));
#10661=CARTESIAN_POINT('Ctrl Pts',(148.504256288339,-2.14439794963443,329.485520151809));
#10662=CARTESIAN_POINT('Ctrl Pts',(148.496832310901,-2.29047088732067,329.542323062817));
#10663=CARTESIAN_POINT('Ctrl Pts',(148.489408333463,-2.43450564796971,329.605019656282));
#10664=CARTESIAN_POINT('Ctrl Pts',(148.481984356025,-2.5759913667248,329.673443979356));
#10665=CARTESIAN_POINT('Ctrl Pts',(148.474569139998,-2.71731011104409,329.741787551434));
#10666=CARTESIAN_POINT('Ctrl Pts',(148.46715392397,-2.85608546872859,329.815845237157));
#10667=CARTESIAN_POINT('Ctrl Pts',(148.459738707943,-2.99182401071739,329.895402106787));
#10668=CARTESIAN_POINT('Ctrl Pts',(148.452330626798,-3.12743194576445,329.974882427197));
#10669=CARTESIAN_POINT('Ctrl Pts',(148.444922545654,-3.26000856245942,330.059851210093));
#10670=CARTESIAN_POINT('Ctrl Pts',(148.43751446451,-3.38908272367766,330.150046510061));
#10671=CARTESIAN_POINT('Ctrl Pts',(148.430111897336,-3.51806081264043,330.240174676021));
#10672=CARTESIAN_POINT('Ctrl Pts',(148.422709330162,-3.64354133231631,330.335521400256));
#10673=CARTESIAN_POINT('Ctrl Pts',(148.415306762988,-3.76508006753448,330.435780170987));
#10674=CARTESIAN_POINT('Ctrl Pts',(148.407908093233,-3.88655481313961,330.535986155913));
#10675=CARTESIAN_POINT('Ctrl Pts',(148.400509423479,-4.00409162026188,330.64109879993));
#10676=CARTESIAN_POINT('Ctrl Pts',(148.393110753724,-4.11727755043953,330.750769936195));
#10677=CARTESIAN_POINT('Ctrl Pts',(148.38571330452,-4.2304448084536,330.860422980127));
#10678=CARTESIAN_POINT('Ctrl Pts',(148.378315855316,-4.33926234627553,330.974632764358));
#10679=CARTESIAN_POINT('Ctrl Pts',(148.370918406112,-4.44335237528694,331.093012639957));
#10680=CARTESIAN_POINT('Ctrl Pts',(148.363521277649,-4.54743789113605,331.211387382812));
#10681=CARTESIAN_POINT('Ctrl Pts',(148.356124149185,-4.64679605929418,331.333931577257));
#10682=CARTESIAN_POINT('Ctrl Pts',(148.348727020722,-4.74108804605963,331.460223919227));
#10683=CARTESIAN_POINT('Ctrl Pts',(148.341328753285,-4.83539455143715,331.586535707066));
#10684=CARTESIAN_POINT('Ctrl Pts',(148.333930485848,-4.92463309891664,331.716596492483));
#10685=CARTESIAN_POINT('Ctrl Pts',(148.326532218412,-5.00850711054575,331.849954431105));
#10686=CARTESIAN_POINT('Ctrl Pts',(148.319131351886,-5.09241058799718,331.983359219774));
#10687=CARTESIAN_POINT('Ctrl Pts',(148.31173048536,-5.1709455787568,332.120063152147));
#10688=CARTESIAN_POINT('Ctrl Pts',(148.304329618834,-5.24386061599907,332.259588278657));
#10689=CARTESIAN_POINT('Ctrl Pts',(148.29692062545,-5.31685572092326,332.399266617095));
#10690=CARTESIAN_POINT('Ctrl Pts',(148.289511632065,-5.38421837506148,332.541772005458));
#10691=CARTESIAN_POINT('Ctrl Pts',(148.28210263868,-5.44574427864021,332.686604267714));
#10692=CARTESIAN_POINT('Ctrl Pts',(148.2746890811,-5.50730808429778,332.83152575164));
#10693=CARTESIAN_POINT('Ctrl Pts',(148.26727552352,-5.56302784283388,332.978776617527));
#10694=CARTESIAN_POINT('Ctrl Pts',(148.259861965939,-5.61274878683966,333.127840386524));
#10695=CARTESIAN_POINT('Ctrl Pts',(148.252437853803,-5.66254051771185,333.277116375086));
#10696=CARTESIAN_POINT('Ctrl Pts',(148.245013741666,-5.70631627356744,333.428210064029));
#10697=CARTESIAN_POINT('Ctrl Pts',(148.237589629529,-5.7439719547281,333.580592818886));
#10698=CARTESIAN_POINT('Ctrl Pts',(148.233732504375,-5.763535597134,333.659761795067));
#10699=CARTESIAN_POINT('Ctrl Pts',(148.22987537922,-5.78144814558562,333.739278589465));
#10700=CARTESIAN_POINT('Ctrl Pts',(148.226018254065,-5.79770052668763,333.819068517929));
#10701=CARTESIAN_POINT('Ctrl Pts',(148.215400427831,-5.84243979531541,334.038712828564));
#10702=CARTESIAN_POINT('Ctrl Pts',(148.204782601597,-5.87470894321651,334.260975959509));
#10703=CARTESIAN_POINT('Ctrl Pts',(148.194164775363,-5.8942673528667,334.484691417275));
#10704=CARTESIAN_POINT('Ctrl Pts',(148.186127185143,-5.90907287695997,334.654041822509));
#10705=CARTESIAN_POINT('Ctrl Pts',(148.178089594923,-5.91659554481408,334.82422426963));
#10706=CARTESIAN_POINT('Ctrl Pts',(148.170052004703,-5.91674764559936,334.994721667458));
#10707=CARTESIAN_POINT('',(146.420052004731,-5.91674999222498,334.999696675565));
#10708=CARTESIAN_POINT('Ctrl Pts',(148.170052004658,-5.91674764560021,334.994721668406));
#10709=CARTESIAN_POINT('Ctrl Pts',(148.162748410747,-5.91688585644941,335.149649168135));
#10710=CARTESIAN_POINT('Ctrl Pts',(148.155444816836,-5.9109348501119,335.304773595374));
#10711=CARTESIAN_POINT('Ctrl Pts',(148.148141222925,-5.89887502142363,335.45956941165));
#10712=CARTESIAN_POINT('Ctrl Pts',(148.140843472054,-5.88682484087063,335.614241387778));
#10713=CARTESIAN_POINT('Ctrl Pts',(148.133545721183,-5.86867559334,335.768584894349));
#10714=CARTESIAN_POINT('Ctrl Pts',(148.126247970312,-5.84445973527854,335.922074273152));
#10715=CARTESIAN_POINT('Ctrl Pts',(148.118811814041,-5.81978461167114,336.078474652802));
#10716=CARTESIAN_POINT('Ctrl Pts',(148.111375657769,-5.78881043696119,336.233987774095));
#10717=CARTESIAN_POINT('Ctrl Pts',(148.103939501497,-5.75162705930377,336.388062222375));
#10718=CARTESIAN_POINT('Ctrl Pts',(148.096647403661,-5.71516402412085,336.539151832366));
#10719=CARTESIAN_POINT('Ctrl Pts',(148.089355305825,-5.67273027635409,336.688857615709));
#10720=CARTESIAN_POINT('Ctrl Pts',(148.082063207988,-5.62446214253966,336.83666985864));
#10721=CARTESIAN_POINT('Ctrl Pts',(148.074771469774,-5.57619638915013,336.98447481196));
#10722=CARTESIAN_POINT('Ctrl Pts',(148.06747973156,-5.52209694138336,337.130386044619));
#10723=CARTESIAN_POINT('Ctrl Pts',(148.060187993346,-5.46234978476907,337.27390971486));
#10724=CARTESIAN_POINT('Ctrl Pts',(148.052895079054,-5.40259299158463,337.417456533916));
#10725=CARTESIAN_POINT('Ctrl Pts',(148.045602164761,-5.3371868253239,337.558614669072));
#10726=CARTESIAN_POINT('Ctrl Pts',(148.038309250468,-5.2663650035639,337.69691123542));
#10727=CARTESIAN_POINT('Ctrl Pts',(148.030765164579,-5.19310404302206,337.839970804329));
#10728=CARTESIAN_POINT('Ctrl Pts',(148.023221078689,-5.11404791220634,337.97996776799));
#10729=CARTESIAN_POINT('Ctrl Pts',(148.015676992799,-5.02950589739266,338.116408347857));
#10730=CARTESIAN_POINT('Ctrl Pts',(148.008373354424,-4.94765843267006,338.248500249996));
#10731=CARTESIAN_POINT('Ctrl Pts',(148.001069716048,-4.86066969174803,338.37725871238));
#10732=CARTESIAN_POINT('Ctrl Pts',(147.993766077673,-4.76886283938269,338.502267520001));
#10733=CARTESIAN_POINT('Ctrl Pts',(147.986101768026,-4.67252234330752,338.63344956393));
#10734=CARTESIAN_POINT('Ctrl Pts',(147.978437458379,-4.57087609919874,338.760501823122));
#10735=CARTESIAN_POINT('Ctrl Pts',(147.970773148732,-4.46434240320478,338.882985638584));
#10736=CARTESIAN_POINT('Ctrl Pts',(147.963108839085,-4.35780870721077,339.005469454045));
#10737=CARTESIAN_POINT('Ctrl Pts',(147.955444529438,-4.24638794587433,339.123384529299));
#10738=CARTESIAN_POINT('Ctrl Pts',(147.947780219791,-4.13053890431873,339.236340274625));
#10739=CARTESIAN_POINT('Ctrl Pts',(147.940356242353,-4.01832257821205,339.345754030517));
#10740=CARTESIAN_POINT('Ctrl Pts',(147.932932264915,-3.90158657809671,339.450871019555));
#10741=CARTESIAN_POINT('Ctrl Pts',(147.925508287477,-3.78069359453069,339.551295036226));
#10742=CARTESIAN_POINT('Ctrl Pts',(147.91809307145,-3.65994328287461,339.651600537447));
#10743=CARTESIAN_POINT('Ctrl Pts',(147.910677855422,-3.53504603726267,339.747223854446));
#10744=CARTESIAN_POINT('Ctrl Pts',(147.903262639394,-3.40640190055357,339.837804941748));
#10745=CARTESIAN_POINT('Ctrl Pts',(147.89585455825,-3.27788154458527,339.928298872385));
#10746=CARTESIAN_POINT('Ctrl Pts',(147.888446477106,-3.1456217779952,340.013760018542));
#10747=CARTESIAN_POINT('Ctrl Pts',(147.881038395962,-3.01005619906946,340.093868102036));
#10748=CARTESIAN_POINT('Ctrl Pts',(147.873635828788,-2.8745915240796,340.173916559621));
#10749=CARTESIAN_POINT('Ctrl Pts',(147.866233261614,-2.73582625605024,340.248619698975));
#10750=CARTESIAN_POINT('Ctrl Pts',(147.85883069444,-2.59422340127637,340.317700208433));
#10751=CARTESIAN_POINT('Ctrl Pts',(147.851432024685,-2.45269509978787,340.386744347304));
#10752=CARTESIAN_POINT('Ctrl Pts',(147.844033354931,-2.30833252147898,340.450171588648));
#10753=CARTESIAN_POINT('Ctrl Pts',(147.836634685176,-2.16162362679046,340.507750344615));
#10754=CARTESIAN_POINT('Ctrl Pts',(147.829237235972,-2.01493893451307,340.565319601875));
#10755=CARTESIAN_POINT('Ctrl Pts',(147.821839786768,-1.86590904113859,340.617042152395));
#10756=CARTESIAN_POINT('Ctrl Pts',(147.814442337564,-1.71504236876553,340.662734342686));
#10757=CARTESIAN_POINT('Ctrl Pts',(147.807045209101,-1.56418223770847,340.708424551844));
#10758=CARTESIAN_POINT('Ctrl Pts',(147.799648080637,-1.41148584319119,340.748084812473));
#10759=CARTESIAN_POINT('Ctrl Pts',(147.792250952174,-1.25747700947135,340.781581283105));
#10760=CARTESIAN_POINT('Ctrl Pts',(147.784852684737,-1.10344446223524,340.815082911358));
#10761=CARTESIAN_POINT('Ctrl Pts',(147.7774544173,-0.948099438130381,340.842418780568));
#10762=CARTESIAN_POINT('Ctrl Pts',(147.770056149864,-0.791976050973206,
340.863506160753));
#10763=CARTESIAN_POINT('Ctrl Pts',(147.762655283338,-0.635797816028739,
340.884600949155));
#10764=CARTESIAN_POINT('Ctrl Pts',(147.755254416812,-0.478841043219018,
340.899442828048));
#10765=CARTESIAN_POINT('Ctrl Pts',(147.747853550287,-0.321644916362601,
340.908000940274));
#10766=CARTESIAN_POINT('Ctrl Pts',(147.740444556902,-0.164276173130186,
340.916568450125));
#10767=CARTESIAN_POINT('Ctrl Pts',(147.733035563517,-0.00666792383998877,
340.918838392987));
#10768=CARTESIAN_POINT('Ctrl Pts',(147.725626570132,0.150639959648062,340.914832048762));
#10769=CARTESIAN_POINT('Ctrl Pts',(147.718213012552,0.308044750218301,340.91082323649));
#10770=CARTESIAN_POINT('Ctrl Pts',(147.710799454972,0.465148434735534,340.900530457142));
#10771=CARTESIAN_POINT('Ctrl Pts',(147.703385897392,0.621416824595331,340.884026826299));
#10772=CARTESIAN_POINT('Ctrl Pts',(147.695961785255,0.777907691116904,340.867499699516));
#10773=CARTESIAN_POINT('Ctrl Pts',(147.688537673118,0.933560519631203,340.84474411527));
#10774=CARTESIAN_POINT('Ctrl Pts',(147.681113560982,1.08785104971144,340.81588433999));
#10775=CARTESIAN_POINT('Ctrl Pts',(147.677256435827,1.16801119192923,340.800890524818));
#10776=CARTESIAN_POINT('Ctrl Pts',(147.673399310672,1.24780385406735,340.784249880222));
#10777=CARTESIAN_POINT('Ctrl Pts',(147.669542185517,1.32715730388919,340.765985089578));
#10778=CARTESIAN_POINT('Ctrl Pts',(147.662118208079,1.47989235848651,340.730830048398));
#10779=CARTESIAN_POINT('Ctrl Pts',(147.654694230641,1.63146002511382,340.689549089827));
#10780=CARTESIAN_POINT('Ctrl Pts',(147.647270253203,1.7813308534301,340.642232798557));
#10781=CARTESIAN_POINT('Ctrl Pts',(147.639855037176,1.93102481161985,340.59497234763));
#10782=CARTESIAN_POINT('Ctrl Pts',(147.632439821148,2.0790255651209,340.541690852922));
#10783=CARTESIAN_POINT('Ctrl Pts',(147.625024605121,2.22481385786861,340.482529877742));
#10784=CARTESIAN_POINT('Ctrl Pts',(147.617616523976,2.37046187385489,340.423425826955));
#10785=CARTESIAN_POINT('Ctrl Pts',(147.610208442832,2.51390132365814,340.358453697536));
#10786=CARTESIAN_POINT('Ctrl Pts',(147.602800361688,2.65462823360733,340.287804790632));
#10787=CARTESIAN_POINT('Ctrl Pts',(147.595397794514,2.79525039794722,340.217208469));
#10788=CARTESIAN_POINT('Ctrl Pts',(147.58799522734,2.93316371043148,340.140943949857));
#10789=CARTESIAN_POINT('Ctrl Pts',(147.580592660166,3.06788441449027,340.05925051582));
#10790=CARTESIAN_POINT('Ctrl Pts',(147.573193990412,3.20253418868727,339.977600093019));
#10791=CARTESIAN_POINT('Ctrl Pts',(147.565795320657,3.3339943837407,339.890526640824));
#10792=CARTESIAN_POINT('Ctrl Pts',(147.558396650902,3.46180618909339,339.798315170104));
#10793=CARTESIAN_POINT('Ctrl Pts',(147.550999201698,3.58959690946702,339.706118911415));
#10794=CARTESIAN_POINT('Ctrl Pts',(147.543601752494,3.71374013229002,339.608786534589));
#10795=CARTESIAN_POINT('Ctrl Pts',(147.53620430329,3.83380628305483,339.506646197175));
#10796=CARTESIAN_POINT('Ctrl Pts',(147.528807174827,3.95386722796063,339.404510288388));
#10797=CARTESIAN_POINT('Ctrl Pts',(147.521410046363,4.0698511680286,339.297567075335));
#10798=CARTESIAN_POINT('Ctrl Pts',(147.5140129179,4.18136208175002,339.186184623712));
#10799=CARTESIAN_POINT('Ctrl Pts',(147.506614650463,4.29289016536814,339.074785021972));
#10800=CARTESIAN_POINT('Ctrl Pts',(147.499216383027,4.39994358721055,338.958945084424));
#10801=CARTESIAN_POINT('Ctrl Pts',(147.49181811559,4.50216373823538,338.839069188829));
#10802=CARTESIAN_POINT('Ctrl Pts',(147.484417249064,4.6044198002745,338.719151179571));
#10803=CARTESIAN_POINT('Ctrl Pts',(147.477016382539,4.70183896881829,338.595194673086));
#10804=CARTESIAN_POINT('Ctrl Pts',(147.469615516013,4.7941035121219,338.46763638197));
#10805=CARTESIAN_POINT('Ctrl Pts',(147.462206522628,4.88646937071502,338.339938019655));
#10806=CARTESIAN_POINT('Ctrl Pts',(147.454797529243,4.97366908134501,338.208630276734));
#10807=CARTESIAN_POINT('Ctrl Pts',(147.447388535859,5.05542838309439,338.074178658748));
#10808=CARTESIAN_POINT('Ctrl Pts',(147.439974978278,5.13723805139403,337.939644213928));
#10809=CARTESIAN_POINT('Ctrl Pts',(147.432561420698,5.21360045195357,337.801962360452));
#10810=CARTESIAN_POINT('Ctrl Pts',(147.425147863118,5.28428798911991,337.661621875951));
#10811=CARTESIAN_POINT('Ctrl Pts',(147.417723750981,5.35507616293637,337.521081591078));
#10812=CARTESIAN_POINT('Ctrl Pts',(147.410299638844,5.42017318354134,337.377875454523));
#10813=CARTESIAN_POINT('Ctrl Pts',(147.402875526708,5.47939984182708,337.232511575756));
#10814=CARTESIAN_POINT('Ctrl Pts',(147.399018401553,5.51017047531185,337.156989188289));
#10815=CARTESIAN_POINT('Ctrl Pts',(147.395161276398,5.53935739024372,337.080884628764));
#10816=CARTESIAN_POINT('Ctrl Pts',(147.391304151243,5.56694084312725,337.004270493626));
#10817=CARTESIAN_POINT('Ctrl Pts',(147.383880173805,5.62003192097725,336.856807917777));
#10818=CARTESIAN_POINT('Ctrl Pts',(147.376456196367,5.667339843588,336.707011937972));
#10819=CARTESIAN_POINT('Ctrl Pts',(147.369032218929,5.70865426959873,336.555376800872));
#10820=CARTESIAN_POINT('Ctrl Pts',(147.361617002902,5.74991993837071,336.403920616049));
#10821=CARTESIAN_POINT('Ctrl Pts',(147.354201786874,5.78520609276058,336.250629950894));
#10822=CARTESIAN_POINT('Ctrl Pts',(147.346786570846,5.81435077712405,336.096018066939));
#10823=CARTESIAN_POINT('Ctrl Pts',(147.339378489702,5.843467418619,335.941554949761));
#10824=CARTESIAN_POINT('Ctrl Pts',(147.331970408558,5.86645428571385,335.785773508945));
#10825=CARTESIAN_POINT('Ctrl Pts',(147.324562327414,5.88319951855191,335.629201070732));
#10826=CARTESIAN_POINT('Ctrl Pts',(147.31715976024,5.89993228760728,335.472745172245));
#10827=CARTESIAN_POINT('Ctrl Pts',(147.309757193066,5.91043263327722,335.31549981816));
#10828=CARTESIAN_POINT('Ctrl Pts',(147.302354625892,5.91463998498093,335.15800129925));
#10829=CARTESIAN_POINT('Ctrl Pts',(147.294955956137,5.91884512153238,335.000585702622));
#10830=CARTESIAN_POINT('Ctrl Pts',(147.287557286382,5.91676385267814,334.842917578764));
#10831=CARTESIAN_POINT('Ctrl Pts',(147.280158616628,5.90838756142093,334.685536986998));
#10832=CARTESIAN_POINT('Ctrl Pts',(147.272761167424,5.90001265199168,334.528182358142));
#10833=CARTESIAN_POINT('Ctrl Pts',(147.26536371822,5.88534480102928,334.371115539559));
#10834=CARTESIAN_POINT('Ctrl Pts',(147.257966269016,5.8644274958022,334.214875354495));
#10835=CARTESIAN_POINT('Ctrl Pts',(147.250569140552,5.84351109751306,334.058641943734));
#10836=CARTESIAN_POINT('Ctrl Pts',(147.243172012089,5.81634583325121,333.903235465139));
#10837=CARTESIAN_POINT('Ctrl Pts',(147.235774883625,5.78302690735014,333.749188123112));
#10838=CARTESIAN_POINT('Ctrl Pts',(147.228376616189,5.74970285116603,333.595117061639));
#10839=CARTESIAN_POINT('Ctrl Pts',(147.220978348752,5.71022332562729,333.442405918224));
#10840=CARTESIAN_POINT('Ctrl Pts',(147.213580081315,5.6647343166913,333.291575086871));
#10841=CARTESIAN_POINT('Ctrl Pts',(147.206179214789,5.61922932698793,333.14069126706));
#10842=CARTESIAN_POINT('Ctrl Pts',(147.198778348264,5.56771075819675,332.991689431601));
#10843=CARTESIAN_POINT('Ctrl Pts',(147.191377481738,5.51037390837914,332.845073098141));
#10844=CARTESIAN_POINT('Ctrl Pts',(147.183968488353,5.45297409721925,332.698295765932));
#10845=CARTESIAN_POINT('Ctrl Pts',(147.176559494968,5.38974338180881,332.553909514807));
#10846=CARTESIAN_POINT('Ctrl Pts',(147.169150501583,5.32092479736872,332.412396888384));
#10847=CARTESIAN_POINT('Ctrl Pts',(147.161736944003,5.25206381830673,332.270797085301));
#10848=CARTESIAN_POINT('Ctrl Pts',(147.154323386423,5.17760828702107,332.132074762451));
#10849=CARTESIAN_POINT('Ctrl Pts',(147.146909828843,5.09784606198155,331.996685815497));
#10850=CARTESIAN_POINT('Ctrl Pts',(147.139485716706,5.01797028081234,331.86110411759));
#10851=CARTESIAN_POINT('Ctrl Pts',(147.132061604569,4.93277291852831,331.728865586523));
#10852=CARTESIAN_POINT('Ctrl Pts',(147.124637492433,4.84258427489381,331.600395890247));
#10853=CARTESIAN_POINT('Ctrl Pts',(147.120780367278,4.79572764347448,331.533650710761));
#10854=CARTESIAN_POINT('Ctrl Pts',(147.116923242124,4.74752441016964,331.467922267288));
#10855=CARTESIAN_POINT('Ctrl Pts',(147.113066116969,4.69802493853934,331.403266448656));
#10856=CARTESIAN_POINT('Ctrl Pts',(147.105642139531,4.60275114112179,331.278820567451));
#10857=CARTESIAN_POINT('Ctrl Pts',(147.098218162093,4.50238553739962,331.157975126094));
#10858=CARTESIAN_POINT('Ctrl Pts',(147.090794184655,4.39722992215444,331.04117447035));
#10859=CARTESIAN_POINT('Ctrl Pts',(147.083378968628,4.29219840635662,330.924511656953));
#10860=CARTESIAN_POINT('Ctrl Pts',(147.0759637526,4.18238837857425,330.811884402198));
#10861=CARTESIAN_POINT('Ctrl Pts',(147.068548536572,4.06814380788774,330.703706653306));
#10862=CARTESIAN_POINT('Ctrl Pts',(147.061140455428,3.95400916275233,330.5956329925));
#10863=CARTESIAN_POINT('Ctrl Pts',(147.053732374284,3.83544873849147,330.492000569195));
#10864=CARTESIAN_POINT('Ctrl Pts',(147.04632429314,3.71284544120223,330.393188815217));
#10865=CARTESIAN_POINT('Ctrl Pts',(147.038921725966,3.590333399786,330.294450608631));
#10866=CARTESIAN_POINT('Ctrl Pts',(147.031519158792,3.46378476640493,330.20052616011));
#10867=CARTESIAN_POINT('Ctrl Pts',(147.024116591618,3.33361774119527,330.111756622458));
#10868=CARTESIAN_POINT('Ctrl Pts',(147.016717921863,3.20351924835548,330.023033821579));
#10869=CARTESIAN_POINT('Ctrl Pts',(147.009319252109,3.06980646530157,329.939460736146));
#10870=CARTESIAN_POINT('Ctrl Pts',(147.001920582354,2.93292887628733,329.861336869463));
#10871=CARTESIAN_POINT('Ctrl Pts',(146.99452313315,2.79607386782491,329.783225890793));
#10872=CARTESIAN_POINT('Ctrl Pts',(146.987125683946,2.65605541340817,329.710562531564));
#10873=CARTESIAN_POINT('Ctrl Pts',(146.979728234742,2.5133501544572,329.643601810583));
#10874=CARTESIAN_POINT('Ctrl Pts',(146.972331106278,2.37065108295752,329.576643992902));
#10875=CARTESIAN_POINT('Ctrl Pts',(146.964933977815,2.22526577642031,329.515388480375));
#10876=CARTESIAN_POINT('Ctrl Pts',(146.957536849351,2.07769329740963,329.460043219988));
#10877=CARTESIAN_POINT('Ctrl Pts',(146.950138581915,1.93009809592073,329.404689437813));
#10878=CARTESIAN_POINT('Ctrl Pts',(146.942740314478,1.78031540087056,329.355247850831));
#10879=CARTESIAN_POINT('Ctrl Pts',(146.935342047042,1.62886182405741,329.311877311395));
#10880=CARTESIAN_POINT('Ctrl Pts',(146.927941180516,1.47735504001039,329.268491535431));
#10881=CARTESIAN_POINT('Ctrl Pts',(146.92054031399,1.3241765640518,329.231181156138));
#10882=CARTESIAN_POINT('Ctrl Pts',(146.913139447464,1.16985550190098,329.200054425499));
#10883=CARTESIAN_POINT('Ctrl Pts',(146.90573045408,1.01536498047001,329.168893514734));
#10884=CARTESIAN_POINT('Ctrl Pts',(146.898321460695,0.859729733267863,329.143929886926));
#10885=CARTESIAN_POINT('Ctrl Pts',(146.89091246731,0.703487061818735,329.125220300611));
#10886=CARTESIAN_POINT('Ctrl Pts',(146.88349890973,0.54714813949461,329.106499188545));
#10887=CARTESIAN_POINT('Ctrl Pts',(146.87608535215,0.390201418463485,329.094039824463));
#10888=CARTESIAN_POINT('Ctrl Pts',(146.868671794569,0.233186047849093,329.087846853338));
#10889=CARTESIAN_POINT('Ctrl Pts',(146.861247682433,0.0759471371091804,
329.081645065384));
#10890=CARTESIAN_POINT('Ctrl Pts',(146.853823570296,-0.081360246206188,
329.081727487929));
#10891=CARTESIAN_POINT('Ctrl Pts',(146.846399458159,-0.238199404679093,
329.088046718206));
#10892=CARTESIAN_POINT('Ctrl Pts',(146.842542333005,-0.31968366195242,329.091329812752));
#10893=CARTESIAN_POINT('Ctrl Pts',(146.83868520785,-0.401041647769633,329.096295507749));
#10894=CARTESIAN_POINT('Ctrl Pts',(146.834828082695,-0.482199109410888,
329.102931696056));
#10895=CARTESIAN_POINT('Ctrl Pts',(146.827404105257,-0.638406424444336,
329.115704657858));
#10896=CARTESIAN_POINT('Ctrl Pts',(146.819980127819,-0.794341521357021,
329.134707832806));
#10897=CARTESIAN_POINT('Ctrl Pts',(146.812556150381,-0.94946742184152,329.159927896219));
#10898=CARTESIAN_POINT('Ctrl Pts',(146.805140934354,-1.10441025042355,329.185118196163));
#10899=CARTESIAN_POINT('Ctrl Pts',(146.797725718326,-1.25854541867509,329.21651072112));
#10900=CARTESIAN_POINT('Ctrl Pts',(146.790310502299,-1.41133868813917,329.254040230748));
#10901=CARTESIAN_POINT('Ctrl Pts',(146.782902421154,-1.56398494068897,329.291533629671));
#10902=CARTESIAN_POINT('Ctrl Pts',(146.77549434001,-1.71529150491061,329.33515216913));
#10903=CARTESIAN_POINT('Ctrl Pts',(146.768086258866,-1.86473209602684,329.384779187552));
#10904=CARTESIAN_POINT('Ctrl Pts',(146.760683691692,-2.01406145578125,329.434369267678));
#10905=CARTESIAN_POINT('Ctrl Pts',(146.753281124518,-2.1615272552138,329.489958804806));
#10906=CARTESIAN_POINT('Ctrl Pts',(146.745878557344,-2.30661629956362,329.551380742877));
#10907=CARTESIAN_POINT('Ctrl Pts',(146.73847988759,-2.45162895516745,329.612770342568));
#10908=CARTESIAN_POINT('Ctrl Pts',(146.731081217835,-2.59426700501119,329.679986082525));
#10909=CARTESIAN_POINT('Ctrl Pts',(146.72368254808,-2.73403534865528,329.752812060274));
#10910=CARTESIAN_POINT('Ctrl Pts',(146.716285098876,-2.87378063486127,329.825626023998));
#10911=CARTESIAN_POINT('Ctrl Pts',(146.708887649672,-3.0106568237829,329.904048216378));
#10912=CARTESIAN_POINT('Ctrl Pts',(146.701490200468,-3.14419152664447,329.987815824785));
#10913=CARTESIAN_POINT('Ctrl Pts',(146.694093072005,-3.27772043967407,330.071579801174));
#10914=CARTESIAN_POINT('Ctrl Pts',(146.686695943541,-3.40790783856087,330.160688534431));
#10915=CARTESIAN_POINT('Ctrl Pts',(146.679298815078,-3.5343087848591,330.254834884246));
#10916=CARTESIAN_POINT('Ctrl Pts',(146.671900547641,-3.66072919374794,330.348995730249));
#10917=CARTESIAN_POINT('Ctrl Pts',(146.664502280204,-3.78336168985092,330.448195514316));
#10918=CARTESIAN_POINT('Ctrl Pts',(146.657104012768,-3.90179312255097,330.552085770688));
#10919=CARTESIAN_POINT('Ctrl Pts',(146.649703146242,-4.02026616145841,330.656012524799));
#10920=CARTESIAN_POINT('Ctrl Pts',(146.642302279716,-4.13453491810818,330.764632786047));
#10921=CARTESIAN_POINT('Ctrl Pts',(146.634901413191,-4.24422203163209,330.877560199505));
#10922=CARTESIAN_POINT('Ctrl Pts',(146.627492419806,-4.35402959209327,330.990611618058));
#10923=CARTESIAN_POINT('Ctrl Pts',(146.620083426421,-4.45924520190224,331.107979366343));
#10924=CARTESIAN_POINT('Ctrl Pts',(146.612674433037,-4.55953036690967,331.229242331344));
#10925=CARTESIAN_POINT('Ctrl Pts',(146.605260875456,-4.65987731103766,331.350579998514));
#10926=CARTESIAN_POINT('Ctrl Pts',(146.597847317876,-4.75528753245377,331.475817367716));
#10927=CARTESIAN_POINT('Ctrl Pts',(146.590433760296,-4.84546536057333,331.604503570612));
#10928=CARTESIAN_POINT('Ctrl Pts',(146.583009648159,-4.93577157334081,331.733372981878));
#10929=CARTESIAN_POINT('Ctrl Pts',(146.575585536023,-5.02083031387259,331.865700720081));
#10930=CARTESIAN_POINT('Ctrl Pts',(146.568161423886,-5.10039100639596,332.001009812558));
#10931=CARTESIAN_POINT('Ctrl Pts',(146.564304298731,-5.14172598932963,332.071308333736));
#10932=CARTESIAN_POINT('Ctrl Pts',(146.560447173576,-5.18157770491679,332.142411222204));
#10933=CARTESIAN_POINT('Ctrl Pts',(146.556590048422,-5.21991615190281,332.214249485398));
#10934=CARTESIAN_POINT('Ctrl Pts',(146.548750793122,-5.2978355508435,332.360254207266));
#10935=CARTESIAN_POINT('Ctrl Pts',(146.540911537823,-5.36971495926341,332.509698015299));
#10936=CARTESIAN_POINT('Ctrl Pts',(146.533072282524,-5.43525564688561,332.6620678762));
#10937=CARTESIAN_POINT('Ctrl Pts',(146.525246388352,-5.50068462779268,332.814178039846));
#10938=CARTESIAN_POINT('Ctrl Pts',(146.517420494179,-5.55979630146954,332.96920403031));
#10939=CARTESIAN_POINT('Ctrl Pts',(146.509594600007,-5.61233759419056,333.126608078555));
#10940=CARTESIAN_POINT('Ctrl Pts',(146.501787024606,-5.66475589880413,333.283643677054));
#10941=CARTESIAN_POINT('Ctrl Pts',(146.493979449205,-5.71063440139223,333.443045935796));
#10942=CARTESIAN_POINT('Ctrl Pts',(146.486171873804,-5.74976815257897,333.60425763334));
#10943=CARTESIAN_POINT('Ctrl Pts',(146.478375127486,-5.78884762537151,333.76524573075));
#10944=CARTESIAN_POINT('Ctrl Pts',(146.470578381168,-5.82120091784066,333.928037964224));
#10945=CARTESIAN_POINT('Ctrl Pts',(146.462781634851,-5.84667224702013,334.092060465436));
#10946=CARTESIAN_POINT('Ctrl Pts',(146.454999902127,-5.87209452802309,334.255767121152));
#10947=CARTESIAN_POINT('Ctrl Pts',(146.447218169403,-5.89066123051592,334.420699012688));
#10948=CARTESIAN_POINT('Ctrl Pts',(146.439436436679,-5.90226727024812,334.586271063306));
#10949=CARTESIAN_POINT('Ctrl Pts',(146.432974959363,-5.91190421938478,334.72375201866));
#10950=CARTESIAN_POINT('Ctrl Pts',(146.426513482047,-5.91674291643995,334.861673996697));
#10951=CARTESIAN_POINT('Ctrl Pts',(146.420052004731,-5.91674999222498,334.999696675565));
#10952=CARTESIAN_POINT('',(144.670052004703,-5.91674753464347,335.005401276743));
#10953=CARTESIAN_POINT('Ctrl Pts',(146.420052004703,-5.91674999222501,334.999696676165));
#10954=CARTESIAN_POINT('Ctrl Pts',(146.412332577533,-5.91675844553942,335.164590239239));
#10955=CARTESIAN_POINT('Ctrl Pts',(146.404613150363,-5.90986946465992,335.329362352071));
#10956=CARTESIAN_POINT('Ctrl Pts',(146.396893723193,-5.89613935317849,335.493428100537));
#10957=CARTESIAN_POINT('Ctrl Pts',(146.389165601203,-5.88239377670883,335.657678645382));
#10958=CARTESIAN_POINT('Ctrl Pts',(146.381437479213,-5.86179171970293,335.821220916174));
#10959=CARTESIAN_POINT('Ctrl Pts',(146.373709357223,-5.83444099740712,335.983477915499));
#10960=CARTESIAN_POINT('Ctrl Pts',(146.365762911967,-5.80631760368707,336.150318755259));
#10961=CARTESIAN_POINT('Ctrl Pts',(146.357816466711,-5.77105872154076,336.315800268683));
#10962=CARTESIAN_POINT('Ctrl Pts',(146.349870021454,-5.72883659731168,336.479311259946));
#10963=CARTESIAN_POINT('Ctrl Pts',(146.342116297545,-5.68763846612262,336.638856697128));
#10964=CARTESIAN_POINT('Ctrl Pts',(146.334362573635,-5.63981109997439,336.796525808012));
#10965=CARTESIAN_POINT('Ctrl Pts',(146.326608849725,-5.58556378549572,336.951770416995));
#10966=CARTESIAN_POINT('Ctrl Pts',(146.318566043796,-5.5292939688721,337.11280300936));
#10967=CARTESIAN_POINT('Ctrl Pts',(146.310523237866,-5.46611644690042,337.271226466518));
#10968=CARTESIAN_POINT('Ctrl Pts',(146.302480431937,-5.39631743291392,337.426456001194));
#10969=CARTESIAN_POINT('Ctrl Pts',(146.294437626007,-5.32651841892745,337.581685535869));
#10970=CARTESIAN_POINT('Ctrl Pts',(146.286394820077,-5.2500981463478,337.733720838905));
#10971=CARTESIAN_POINT('Ctrl Pts',(146.278352014148,-5.16739318762945,337.882009404381));
#10972=CARTESIAN_POINT('Ctrl Pts',(146.27092803671,-5.09105170271556,338.018888371007));
#10973=CARTESIAN_POINT('Ctrl Pts',(146.263504059272,-5.00915262107096,338.15293841962));
#10974=CARTESIAN_POINT('Ctrl Pts',(146.256080081834,-4.92193053874683,338.283676344321));
#10975=CARTESIAN_POINT('Ctrl Pts',(146.248664865806,-4.83481139160302,338.414259978599));
#10976=CARTESIAN_POINT('Ctrl Pts',(146.241249649779,-4.74238195319509,338.541538962061));
#10977=CARTESIAN_POINT('Ctrl Pts',(146.233834433751,-4.64492293506497,338.66505409098));
#10978=CARTESIAN_POINT('Ctrl Pts',(146.226426352607,-4.54755769151149,338.788450374263));
#10979=CARTESIAN_POINT('Ctrl Pts',(146.219018271463,-4.44517273228715,338.908089721829));
#10980=CARTESIAN_POINT('Ctrl Pts',(146.211610190318,-4.33809227434411,339.023541472605));
#10981=CARTESIAN_POINT('Ctrl Pts',(146.204207623144,-4.23109151834172,339.138907290536));
#10982=CARTESIAN_POINT('Ctrl Pts',(146.19680505597,-4.11940247527218,339.250091445427));
#10983=CARTESIAN_POINT('Ctrl Pts',(146.189402488796,-4.0033898050446,339.35669606828));
#10984=CARTESIAN_POINT('Ctrl Pts',(146.182003819042,-3.88743821498054,339.463244564265));
#10985=CARTESIAN_POINT('Ctrl Pts',(146.174605149287,-3.76716780540146,339.565218078183));
#10986=CARTESIAN_POINT('Ctrl Pts',(146.167206479532,-3.64298019694015,339.662255446369));
#10987=CARTESIAN_POINT('Ctrl Pts',(146.159809030328,-3.51881307557818,339.759276806403));
#10988=CARTESIAN_POINT('Ctrl Pts',(146.152411581124,-3.39073033165982,339.851363407286));
#10989=CARTESIAN_POINT('Ctrl Pts',(146.14501413192,-3.25916687131794,339.938194190937));
#10990=CARTESIAN_POINT('Ctrl Pts',(146.137617003456,-3.12760911533824,340.025021209757));
#10991=CARTESIAN_POINT('Ctrl Pts',(146.130219874993,-2.99257125449617,340.106592658875));
#10992=CARTESIAN_POINT('Ctrl Pts',(146.122822746529,-2.85451716679003,340.182630828739));
#10993=CARTESIAN_POINT('Ctrl Pts',(146.115424479093,-2.71644182220059,340.258680706584));
#10994=CARTESIAN_POINT('Ctrl Pts',(146.108026211656,-2.57534965294356,340.329195428693));
#10995=CARTESIAN_POINT('Ctrl Pts',(146.100627944219,-2.43172897941287,340.393943337966));
#10996=CARTESIAN_POINT('Ctrl Pts',(146.093227077694,-2.28805785043014,340.458713993859));
#10997=CARTESIAN_POINT('Ctrl Pts',(146.085826211168,-2.14185678860945,340.51771364998));
#10998=CARTESIAN_POINT('Ctrl Pts',(146.078425344642,-1.99363377125032,340.570758920347));
#10999=CARTESIAN_POINT('Ctrl Pts',(146.071016351257,-1.84524799084639,340.623862439494));
#11000=CARTESIAN_POINT('Ctrl Pts',(146.063607357873,-1.69483617244212,340.670998389356));
#11001=CARTESIAN_POINT('Ctrl Pts',(146.056198364488,-1.54292182573692,340.712033158357));
#11002=CARTESIAN_POINT('Ctrl Pts',(146.048784806908,-1.39091389455423,340.75309320619));
#11003=CARTESIAN_POINT('Ctrl Pts',(146.041371249327,-1.23740195372028,340.788044501119));
#11004=CARTESIAN_POINT('Ctrl Pts',(146.033957691747,-1.08291885280208,340.816804734624));
#11005=CARTESIAN_POINT('Ctrl Pts',(146.02653357961,-0.928215816907973,340.845605913587));
#11006=CARTESIAN_POINT('Ctrl Pts',(146.019109467474,-0.772539227898603,
340.868198374132));
#11007=CARTESIAN_POINT('Ctrl Pts',(146.011685355337,-0.616427011310677,
340.884551665355));
#11008=CARTESIAN_POINT('Ctrl Pts',(146.007828230182,-0.535320429616164,
340.893047858539));
#11009=CARTESIAN_POINT('Ctrl Pts',(146.003971105028,-0.454096273587397,
340.899860821188));
#11010=CARTESIAN_POINT('Ctrl Pts',(146.000113979873,-0.372829765666778,
340.904991831352));
#11011=CARTESIAN_POINT('Ctrl Pts',(145.992690002435,-0.216412564486505,
340.914867710968));
#11012=CARTESIAN_POINT('Ctrl Pts',(145.985266024998,-0.0593667263293222,
340.918539199068));
#11013=CARTESIAN_POINT('Ctrl Pts',(145.97784204756,0.0977744572697015,340.915942082036));
#11014=CARTESIAN_POINT('Ctrl Pts',(145.970426831532,0.254730190628689,340.913348029993));
#11015=CARTESIAN_POINT('Ctrl Pts',(145.963011615504,0.411780675921287,340.904500104558));
#11016=CARTESIAN_POINT('Ctrl Pts',(145.955596399477,0.568387849815455,340.88938586057));
#11017=CARTESIAN_POINT('Ctrl Pts',(145.948188318333,0.724844337075537,340.874286159432));
#11018=CARTESIAN_POINT('Ctrl Pts',(145.940780237189,0.880857993120239,340.852932178805));
#11019=CARTESIAN_POINT('Ctrl Pts',(145.933372156045,1.03589121347152,340.825363504225));
#11020=CARTESIAN_POINT('Ctrl Pts',(145.925969588871,1.19080903976526,340.797815349513));
#11021=CARTESIAN_POINT('Ctrl Pts',(145.918567021697,1.34474751754345,340.764061776372));
#11022=CARTESIAN_POINT('Ctrl Pts',(145.911164454523,1.49717473187592,340.724194125354));
#11023=CARTESIAN_POINT('Ctrl Pts',(145.903765784768,1.64952169394666,340.684347464479));
#11024=CARTESIAN_POINT('Ctrl Pts',(145.896367115013,1.80035861704678,340.638393230828));
#11025=CARTESIAN_POINT('Ctrl Pts',(145.888968445259,1.94916445097795,340.586473709376));
#11026=CARTESIAN_POINT('Ctrl Pts',(145.881570996055,2.09794573656686,340.534562753032));
#11027=CARTESIAN_POINT('Ctrl Pts',(145.874173546851,2.24469624595006,340.476688584811));
#11028=CARTESIAN_POINT('Ctrl Pts',(145.866776097647,2.38891064187642,340.41304318361));
#11029=CARTESIAN_POINT('Ctrl Pts',(145.859378969183,2.53311878491825,340.349400541963));
#11030=CARTESIAN_POINT('Ctrl Pts',(145.85198184072,2.67479069170389,340.279987315561));
#11031=CARTESIAN_POINT('Ctrl Pts',(145.844584712256,2.81344179934591,340.205043304738));
#11032=CARTESIAN_POINT('Ctrl Pts',(145.83718644482,2.95211425579716,340.130087754408));
#11033=CARTESIAN_POINT('Ctrl Pts',(145.829788177383,3.0877646586355,340.049599901478));
#11034=CARTESIAN_POINT('Ctrl Pts',(145.822389909947,3.21993394427832,339.963865022035));
#11035=CARTESIAN_POINT('Ctrl Pts',(145.814989043421,3.35214966238097,339.878100023028));
#11036=CARTESIAN_POINT('Ctrl Pts',(145.807588176895,3.48088151548179,339.787084530407));
#11037=CARTESIAN_POINT('Ctrl Pts',(145.80018731037,3.60570039473357,339.691146472443));
#11038=CARTESIAN_POINT('Ctrl Pts',(145.792778316985,3.73065633704814,339.59510306532));
#11039=CARTESIAN_POINT('Ctrl Pts',(145.7853693236,3.85169042845558,339.49412652546));
#11040=CARTESIAN_POINT('Ctrl Pts',(145.777960330215,3.96840701099144,339.388584778447));
#11041=CARTESIAN_POINT('Ctrl Pts',(145.770546772635,4.0851954949682,339.282978014076));
#11042=CARTESIAN_POINT('Ctrl Pts',(145.763133215055,4.19766090422563,339.172800699187));
#11043=CARTESIAN_POINT('Ctrl Pts',(145.755719657475,4.30544566829836,339.058456376485));
#11044=CARTESIAN_POINT('Ctrl Pts',(145.748295545338,4.41338388371535,338.943949263706));
#11045=CARTESIAN_POINT('Ctrl Pts',(145.740871433202,4.51662790080987,338.82526357555));
#11046=CARTESIAN_POINT('Ctrl Pts',(145.733447321065,4.61486101039442,338.702835186346));
#11047=CARTESIAN_POINT('Ctrl Pts',(145.72959019591,4.66589706575485,338.639228709105));
#11048=CARTESIAN_POINT('Ctrl Pts',(145.725733070755,4.71558128286669,338.574612468472));
#11049=CARTESIAN_POINT('Ctrl Pts',(145.721875945601,4.76387402928941,338.509050412229));
#11050=CARTESIAN_POINT('Ctrl Pts',(145.714451968163,4.85682518992741,338.38286025588));
#11051=CARTESIAN_POINT('Ctrl Pts',(145.707027990725,4.94489913691349,338.252783913028));
#11052=CARTESIAN_POINT('Ctrl Pts',(145.699604013287,5.02775327699906,338.119235090231));
#11053=CARTESIAN_POINT('Ctrl Pts',(145.692188797259,5.1105096367333,337.985843875138));
#11054=CARTESIAN_POINT('Ctrl Pts',(145.684773581231,5.18805825661972,337.848988651383));
#11055=CARTESIAN_POINT('Ctrl Pts',(145.677358365204,5.26009749431416,337.70911515311));
#11056=CARTESIAN_POINT('Ctrl Pts',(145.66995028406,5.33206741621664,337.569376240413));
#11057=CARTESIAN_POINT('Ctrl Pts',(145.662542202915,5.3985383396877,337.426625164432));
#11058=CARTESIAN_POINT('Ctrl Pts',(145.655134121771,5.45925262441788,337.281335430244));
#11059=CARTESIAN_POINT('Ctrl Pts',(145.647731554597,5.51992171839747,337.136153837858));
#11060=CARTESIAN_POINT('Ctrl Pts',(145.640328987423,5.5748425619563,336.988437692554));
#11061=CARTESIAN_POINT('Ctrl Pts',(145.632926420249,5.62380411562351,336.838683722557));
#11062=CARTESIAN_POINT('Ctrl Pts',(145.625527750494,5.6727398912467,336.689008597371));
#11063=CARTESIAN_POINT('Ctrl Pts',(145.61812908074,5.7157225098888,336.537298138089));
#11064=CARTESIAN_POINT('Ctrl Pts',(145.610730410985,5.75258965186223,336.384067505502));
#11065=CARTESIAN_POINT('Ctrl Pts',(145.603332961781,5.78945071190187,336.230862151213));
#11066=CARTESIAN_POINT('Ctrl Pts',(145.595935512577,5.82019821032344,336.076137483844));
#11067=CARTESIAN_POINT('Ctrl Pts',(145.588538063373,5.84472011929416,335.920422343068));
#11068=CARTESIAN_POINT('Ctrl Pts',(145.581140934909,5.86924096503766,335.764713953828));
#11069=CARTESIAN_POINT('Ctrl Pts',(145.573743806446,5.88753669998392,335.608015545238));
#11070=CARTESIAN_POINT('Ctrl Pts',(145.566346677982,5.89954675256604,335.450864366287));
#11071=CARTESIAN_POINT('Ctrl Pts',(145.558948410546,5.91155865439647,335.293688989977));
#11072=CARTESIAN_POINT('Ctrl Pts',(145.551550143109,5.91728291832859,335.136061076643));
#11073=CARTESIAN_POINT('Ctrl Pts',(145.544151875672,5.91671101346509,334.978521041905));
#11074=CARTESIAN_POINT('Ctrl Pts',(145.536751009147,5.91613890768541,334.820925661695));
#11075=CARTESIAN_POINT('Ctrl Pts',(145.529350142621,5.90926623055444,334.663418594523));
#11076=CARTESIAN_POINT('Ctrl Pts',(145.521949276095,5.89613652853275,334.506538147977));
#11077=CARTESIAN_POINT('Ctrl Pts',(145.51454028271,5.88299240884299,334.349485431702));
#11078=CARTESIAN_POINT('Ctrl Pts',(145.507131289326,5.86357757402966,334.193061082338));
#11079=CARTESIAN_POINT('Ctrl Pts',(145.499722295941,5.83798730733733,334.037796922751));
#11080=CARTESIAN_POINT('Ctrl Pts',(145.49230873836,5.81238127615806,333.882437115086));
#11081=CARTESIAN_POINT('Ctrl Pts',(145.48489518078,5.7805923077503,333.728239286037));
#11082=CARTESIAN_POINT('Ctrl Pts',(145.4774816232,5.74276624788869,333.575722504352));
#11083=CARTESIAN_POINT('Ctrl Pts',(145.470057511063,5.70488633570577,333.422988587105));
#11084=CARTESIAN_POINT('Ctrl Pts',(145.462633398927,5.66095227027687,333.27194085447));
#11085=CARTESIAN_POINT('Ctrl Pts',(145.45520928679,5.61115919811044,333.123081510571));
#11086=CARTESIAN_POINT('Ctrl Pts',(145.451352161635,5.58528969241902,333.045743088243));
#11087=CARTESIAN_POINT('Ctrl Pts',(145.447495036481,5.55783949790399,332.968995014626));
#11088=CARTESIAN_POINT('Ctrl Pts',(145.443637911326,5.52884094223238,332.8929052233));
#11089=CARTESIAN_POINT('Ctrl Pts',(145.436213933888,5.47302615416728,332.746451874904));
#11090=CARTESIAN_POINT('Ctrl Pts',(145.42878995645,5.41130404880225,332.601996841012));
#11091=CARTESIAN_POINT('Ctrl Pts',(145.421365979012,5.34383712394275,332.460052095953));
#11092=CARTESIAN_POINT('Ctrl Pts',(145.413950762985,5.27644982020538,332.31827486705));
#11093=CARTESIAN_POINT('Ctrl Pts',(145.406535546957,5.20333135083097,332.179002363835));
#11094=CARTESIAN_POINT('Ctrl Pts',(145.399120330929,5.12469330719028,332.042729456113));
#11095=CARTESIAN_POINT('Ctrl Pts',(145.391712249785,5.04613092867937,331.906587669497));
#11096=CARTESIAN_POINT('Ctrl Pts',(145.384304168641,4.96205973421642,331.773440053587));
#11097=CARTESIAN_POINT('Ctrl Pts',(145.376896087497,4.87273848036978,331.643759504382));
#11098=CARTESIAN_POINT('Ctrl Pts',(145.369493520323,4.78348370996359,331.514175478779));
#11099=CARTESIAN_POINT('Ctrl Pts',(145.362090953149,4.68898687179859,331.388053687571));
#11100=CARTESIAN_POINT('Ctrl Pts',(145.354688385975,4.58955146967069,331.265840406498));
#11101=CARTESIAN_POINT('Ctrl Pts',(145.34728971622,4.49016841984711,331.143691470183));
#11102=CARTESIAN_POINT('Ctrl Pts',(145.339891046465,4.38585221932509,331.02544723451));
#11103=CARTESIAN_POINT('Ctrl Pts',(145.332492376711,4.27694823730927,330.911522980635));
#11104=CARTESIAN_POINT('Ctrl Pts',(145.325094927507,4.16806222106933,330.797617520724));
#11105=CARTESIAN_POINT('Ctrl Pts',(145.317697478303,4.05459018305988,330.68803089772));
#11106=CARTESIAN_POINT('Ctrl Pts',(145.310300029099,3.9369162111551,330.583143503707));
#11107=CARTESIAN_POINT('Ctrl Pts',(145.302902900635,3.81924734138875,330.478260657429));
#11108=CARTESIAN_POINT('Ctrl Pts',(145.295505772172,3.69737717858029,330.37807688335));
#11109=CARTESIAN_POINT('Ctrl Pts',(145.288108643708,3.57172472811626,330.282933853648));
#11110=CARTESIAN_POINT('Ctrl Pts',(145.280710376272,3.44605293031148,330.187776174294));
#11111=CARTESIAN_POINT('Ctrl Pts',(145.273312108835,3.31659798281694,330.097661010039));
#11112=CARTESIAN_POINT('Ctrl Pts',(145.265913841398,3.18380971609918,330.012887984597));
#11113=CARTESIAN_POINT('Ctrl Pts',(145.258512974873,3.05097479946708,329.928085177501));
#11114=CARTESIAN_POINT('Ctrl Pts',(145.251112108347,2.91480454646711,329.848628446522));
#11115=CARTESIAN_POINT('Ctrl Pts',(145.243711241821,2.77577519692348,329.774772481638));
#11116=CARTESIAN_POINT('Ctrl Pts',(145.236302248437,2.63659317986197,329.700835415844));
#11117=CARTESIAN_POINT('Ctrl Pts',(145.228893255052,2.49454612617375,329.632511573567));
#11118=CARTESIAN_POINT('Ctrl Pts',(145.221484261667,2.3501328202853,329.570008628965));
#11119=CARTESIAN_POINT('Ctrl Pts',(145.214070704087,2.20563055081888,329.507467180393));
#11120=CARTESIAN_POINT('Ctrl Pts',(145.206657146507,2.05875947184938,329.450753908947));
#11121=CARTESIAN_POINT('Ctrl Pts',(145.199243588926,1.91003500487676,329.400027067686));
#11122=CARTESIAN_POINT('Ctrl Pts',(145.19181947679,1.76109880139785,329.349228007481));
#11123=CARTESIAN_POINT('Ctrl Pts',(145.184395364653,1.6103042968242,329.304432505147));
#11124=CARTESIAN_POINT('Ctrl Pts',(145.176971252516,1.45817941028974,329.265748229289));
#11125=CARTESIAN_POINT('Ctrl Pts',(145.173114127362,1.37914440708806,329.245650190526));
#11126=CARTESIAN_POINT('Ctrl Pts',(145.169257002207,1.29975043929005,329.22720085828));
#11127=CARTESIAN_POINT('Ctrl Pts',(145.165399877052,1.22007212804745,329.210409810283));
#11128=CARTESIAN_POINT('Ctrl Pts',(145.157975899614,1.06671179846213,329.178091346015));
#11129=CARTESIAN_POINT('Ctrl Pts',(145.150551922176,0.911835105823138,329.151821873533));
#11130=CARTESIAN_POINT('Ctrl Pts',(145.143127944738,0.75596051715238,329.131741803652));
#11131=CARTESIAN_POINT('Ctrl Pts',(145.135712728711,0.600269883949183,329.111685431275));
#11132=CARTESIAN_POINT('Ctrl Pts',(145.128297512683,0.44358406543299,329.097803969142));
#11133=CARTESIAN_POINT('Ctrl Pts',(145.120882296656,0.286433712411587,329.090187288002));
#11134=CARTESIAN_POINT('Ctrl Pts',(145.113474215512,0.129434568667987,329.082577935594));
#11135=CARTESIAN_POINT('Ctrl Pts',(145.106066134367,-0.028027849459076,
329.081221381621));
#11136=CARTESIAN_POINT('Ctrl Pts',(145.098658053223,-0.185415845606974,
329.086155943323));
#11137=CARTESIAN_POINT('Ctrl Pts',(145.091255486049,-0.342686694995031,
329.09108683214));
#11138=CARTESIAN_POINT('Ctrl Pts',(145.083852918875,-0.499882861270552,
329.102299501265));
#11139=CARTESIAN_POINT('Ctrl Pts',(145.076450351701,-0.656464818324627,
329.11978023329));
#11140=CARTESIAN_POINT('Ctrl Pts',(145.069051681946,-0.812964335664323,
329.137251761787));
#11141=CARTESIAN_POINT('Ctrl Pts',(145.061653012192,-0.968849917837054,
329.160984739519));
#11142=CARTESIAN_POINT('Ctrl Pts',(145.054254342437,-1.12358544696739,329.190913470617));
#11143=CARTESIAN_POINT('Ctrl Pts',(145.046856893233,-1.27829544953845,329.220837264402));
#11144=CARTESIAN_POINT('Ctrl Pts',(145.039459444029,-1.43185540954218,329.256954712197));
#11145=CARTESIAN_POINT('Ctrl Pts',(145.032061994825,-1.58373759517044,329.299148678299));
#11146=CARTESIAN_POINT('Ctrl Pts',(145.024664866361,-1.7356131954517,329.341340814943));
#11147=CARTESIAN_POINT('Ctrl Pts',(145.017267737898,-1.88581080640624,329.389608846136));
#11148=CARTESIAN_POINT('Ctrl Pts',(145.009870609434,-2.03381636075276,329.443785319731));
#11149=CARTESIAN_POINT('Ctrl Pts',(145.002472341998,-2.18184470426047,329.497970135151));
#11150=CARTESIAN_POINT('Ctrl Pts',(144.995074074561,-2.32767996861832,329.558065076114));
#11151=CARTESIAN_POINT('Ctrl Pts',(144.987675807125,-2.47082676477559,329.623854014169));
#11152=CARTESIAN_POINT('Ctrl Pts',(144.980274940599,-2.61402384990777,329.68966606457));
#11153=CARTESIAN_POINT('Ctrl Pts',(144.972874074073,-2.75453024746913,329.761175939024));
#11154=CARTESIAN_POINT('Ctrl Pts',(144.965473207547,-2.89187406252918,329.838120984664));
#11155=CARTESIAN_POINT('Ctrl Pts',(144.958064214162,-3.02936869422832,329.915150523319));
#11156=CARTESIAN_POINT('Ctrl Pts',(144.950655220778,-3.16369348223284,329.997626969729));
#11157=CARTESIAN_POINT('Ctrl Pts',(144.943246227393,-3.29440386804054,330.085243269831));
#11158=CARTESIAN_POINT('Ctrl Pts',(144.935832669813,-3.42519477595524,330.172913544597));
#11159=CARTESIAN_POINT('Ctrl Pts',(144.928419112232,-3.55236654413012,330.265729762873));
#11160=CARTESIAN_POINT('Ctrl Pts',(144.921005554652,-3.67550717004287,330.363344135537));
#11161=CARTESIAN_POINT('Ctrl Pts',(144.913581442515,-3.79882310917973,330.46109748013));
#11162=CARTESIAN_POINT('Ctrl Pts',(144.906157330379,-3.918096161774,330.563662379406));
#11163=CARTESIAN_POINT('Ctrl Pts',(144.898733218242,-4.03295009966337,330.670653160565));
#11164=CARTESIAN_POINT('Ctrl Pts',(144.894876093087,-4.09262134449154,330.726239178896));
#11165=CARTESIAN_POINT('Ctrl Pts',(144.891018967933,-4.15110041317695,330.783019267912));
#11166=CARTESIAN_POINT('Ctrl Pts',(144.887161842778,-4.20833886981271,330.840935860158));
#11167=CARTESIAN_POINT('Ctrl Pts',(144.879838375853,-4.31701668741422,330.950901243888));
#11168=CARTESIAN_POINT('Ctrl Pts',(144.872514908928,-4.42156715453316,331.065317389096));
#11169=CARTESIAN_POINT('Ctrl Pts',(144.865191442003,-4.52159625809774,331.18383728842));
#11170=CARTESIAN_POINT('Ctrl Pts',(144.857876798109,-4.62150485043848,331.302214399518));
#11171=CARTESIAN_POINT('Ctrl Pts',(144.850562154216,-4.71690267209603,331.42468513694));
#11172=CARTESIAN_POINT('Ctrl Pts',(144.843247510322,-4.80743116996394,331.550864440391));
#11173=CARTESIAN_POINT('Ctrl Pts',(144.83594119061,-4.89785664495903,331.676900149785));
#11174=CARTESIAN_POINT('Ctrl Pts',(144.828634870898,-4.98342360892149,331.806635710497));
#11175=CARTESIAN_POINT('Ctrl Pts',(144.821328551186,-5.06381289989766,331.939652065969));
#11176=CARTESIAN_POINT('Ctrl Pts',(144.814026936671,-5.14415042097581,332.07258276024));
#11177=CARTESIAN_POINT('Ctrl Pts',(144.806725322155,-5.21931670374757,332.208789719243));
#11178=CARTESIAN_POINT('Ctrl Pts',(144.79942370764,-5.28903506488595,332.347823790751));
#11179=CARTESIAN_POINT('Ctrl Pts',(144.792125261801,-5.35872317040015,332.486797525748));
#11180=CARTESIAN_POINT('Ctrl Pts',(144.784826815961,-5.42296788641329,332.62859558944));
#11181=CARTESIAN_POINT('Ctrl Pts',(144.777528370122,-5.48153793665166,332.772743299135));
#11182=CARTESIAN_POINT('Ctrl Pts',(144.770231559051,-5.54009486787256,332.916858721401));
#11183=CARTESIAN_POINT('Ctrl Pts',(144.762934747979,-5.59297951911299,333.063322386253));
#11184=CARTESIAN_POINT('Ctrl Pts',(144.755637936908,-5.64000844513282,333.211638934295));
#11185=CARTESIAN_POINT('Ctrl Pts',(144.748338731286,-5.68705280435101,333.360004154481));
#11186=CARTESIAN_POINT('Ctrl Pts',(144.741039525664,-5.728237476805,333.510223107999));
#11187=CARTESIAN_POINT('Ctrl Pts',(144.733740320043,-5.76342861060435,333.661784317471));
#11188=CARTESIAN_POINT('Ctrl Pts',(144.726440090971,-5.79862467869001,333.813366777932));
#11189=CARTESIAN_POINT('Ctrl Pts',(144.719139861899,-5.82782545587922,333.96629149277));
#11190=CARTESIAN_POINT('Ctrl Pts',(144.711839632827,-5.8509482308236,334.120036726492));
#11191=CARTESIAN_POINT('Ctrl Pts',(144.704532809083,-5.87409189375922,334.273920846188));
#11192=CARTESIAN_POINT('Ctrl Pts',(144.697225985339,-5.89114653610034,334.428626584007));
#11193=CARTESIAN_POINT('Ctrl Pts',(144.689919161595,-5.90208129648768,334.583626451188));
#11194=CARTESIAN_POINT('Ctrl Pts',(144.683296775964,-5.91199178599715,334.72410731252));
#11195=CARTESIAN_POINT('Ctrl Pts',(144.676674390334,-5.91687585969667,334.864829523397));
#11196=CARTESIAN_POINT('Ctrl Pts',(144.670052004703,-5.91674753464347,335.005401276743));
#11197=CARTESIAN_POINT('',(142.920052004703,-5.92143889851083,334.997534891889));
#11198=CARTESIAN_POINT('Ctrl Pts',(144.670052004703,-5.91752625365133,335.00540198762));
#11199=CARTESIAN_POINT('Ctrl Pts',(144.649675939304,-5.9215386892976,335.437980671748));
#11200=CARTESIAN_POINT('Ctrl Pts',(144.536553862478,-5.68061954799383,337.83510250118));
#11201=CARTESIAN_POINT('Ctrl Pts',(144.330685774231,-2.41448809603895,341.566800602679));
#11202=CARTESIAN_POINT('Ctrl Pts',(144.052447739956,4.21554467127444,340.584067159849));
#11203=CARTESIAN_POINT('Ctrl Pts',(143.774209705683,6.97703431509326,334.476917705129));
#11204=CARTESIAN_POINT('Ctrl Pts',(143.495971671408,3.33580254881362,328.849793151726));
#11205=CARTESIAN_POINT('Ctrl Pts',(143.217733637134,-3.36664598015081,328.866622646082));
#11206=CARTESIAN_POINT('Ctrl Pts',(143.025760414899,-5.85942263800703,332.76168318681));
#11207=CARTESIAN_POINT('Ctrl Pts',(142.926533204089,-5.92597114832854,334.860405114397));
#11208=CARTESIAN_POINT('Ctrl Pts',(142.920052004703,-5.92525056693463,334.997533305083));
#11209=CARTESIAN_POINT('',(141.170052034586,-5.91294937614417,334.995918982415));
#11210=CARTESIAN_POINT('Ctrl Pts',(142.920052004703,-5.9167494872914,334.997536844101));
#11211=CARTESIAN_POINT('Ctrl Pts',(142.912703801634,-5.91681411766519,335.152785535897));
#11212=CARTESIAN_POINT('Ctrl Pts',(142.905355598564,-5.91076423044876,335.308283265996));
#11213=CARTESIAN_POINT('Ctrl Pts',(142.898007395495,-5.89856727785858,335.463502568575));
#11214=CARTESIAN_POINT('Ctrl Pts',(142.890667476036,-5.88638407486273,335.618546892821));
#11215=CARTESIAN_POINT('Ctrl Pts',(142.883327556578,-5.86806762495496,335.773313037574));
#11216=CARTESIAN_POINT('Ctrl Pts',(142.87598763712,-5.84363735587839,335.927271813161));
#11217=CARTESIAN_POINT('Ctrl Pts',(142.868654312993,-5.81922903877642,336.081092248104));
#11218=CARTESIAN_POINT('Ctrl Pts',(142.861320988866,-5.78871789525807,336.234106383423));
#11219=CARTESIAN_POINT('Ctrl Pts',(142.85398766474,-5.75217527315325,336.38578865251));
#11220=CARTESIAN_POINT('Ctrl Pts',(142.846659253752,-5.7156571336669,336.537369298371));
#11221=CARTESIAN_POINT('Ctrl Pts',(142.839330842764,-5.67311564843692,336.687619484875));
#11222=CARTESIAN_POINT('Ctrl Pts',(142.832002431776,-5.62467346985876,336.836022581552));
#11223=CARTESIAN_POINT('Ctrl Pts',(142.824676508245,-5.57624773383889,336.984375306287));
#11224=CARTESIAN_POINT('Ctrl Pts',(142.817350584714,-5.52192540487572,337.130881825851));
#11225=CARTESIAN_POINT('Ctrl Pts',(142.810024661183,-5.46187932651101,337.275039512873));
#11226=CARTESIAN_POINT('Ctrl Pts',(142.802699862899,-5.4018424711084,337.419175057551));
#11227=CARTESIAN_POINT('Ctrl Pts',(142.795375064616,-5.33608376158648,337.560962135352));
#11228=CARTESIAN_POINT('Ctrl Pts',(142.788050266333,-5.26482452840527,337.699917266807));
#11229=CARTESIAN_POINT('Ctrl Pts',(142.780725077479,-5.19356149555998,337.838879807587));
#11230=CARTESIAN_POINT('Ctrl Pts',(142.773399888624,-5.11679752930673,337.975009762055));
#11231=CARTESIAN_POINT('Ctrl Pts',(142.76607469977,-5.034800216519,338.107847702549));
#11232=CARTESIAN_POINT('Ctrl Pts',(142.758747604471,-4.9527815632026,338.240720215297));
#11233=CARTESIAN_POINT('Ctrl Pts',(142.751420509171,-4.86552705324495,338.370298684702));
#11234=CARTESIAN_POINT('Ctrl Pts',(142.744093413872,-4.77334779151031,338.496152374223));
#11235=CARTESIAN_POINT('Ctrl Pts',(142.736758692233,-4.68107258584562,338.62213705739));
#11236=CARTESIAN_POINT('Ctrl Pts',(142.729423970594,-4.58386261690172,338.744388909976));
#11237=CARTESIAN_POINT('Ctrl Pts',(142.722089248956,-4.48206990839239,338.862509533811));
#11238=CARTESIAN_POINT('Ctrl Pts',(142.714750479452,-4.38022102281612,338.980695345716));
#11239=CARTESIAN_POINT('Ctrl Pts',(142.707411709948,-4.27378461970932,339.09474510919));
#11240=CARTESIAN_POINT('Ctrl Pts',(142.700072940444,-4.16314930902,339.204297609983));
#11241=CARTESIAN_POINT('Ctrl Pts',(142.692723289544,-4.05234995630737,339.314012547286));
#11242=CARTESIAN_POINT('Ctrl Pts',(142.685373638645,-3.93733954111777,339.419216645527));
#11243=CARTESIAN_POINT('Ctrl Pts',(142.678023987745,-3.81854009505559,339.519588709712));
#11244=CARTESIAN_POINT('Ctrl Pts',(142.672435181359,-3.72820286518126,339.595913427846));
#11245=CARTESIAN_POINT('Ctrl Pts',(142.666846374973,-3.63567536819131,339.669444924152));
#11246=CARTESIAN_POINT('Ctrl Pts',(142.661257568587,-3.5411536962794,339.740059183368));
#11247=CARTESIAN_POINT('Ctrl Pts',(142.653833591149,-3.41559437087036,339.833860727204));
#11248=CARTESIAN_POINT('Ctrl Pts',(142.646409613711,-3.28611599859085,339.922811422643));
#11249=CARTESIAN_POINT('Ctrl Pts',(142.638985636273,-3.15312996209623,340.006565889373));
#11250=CARTESIAN_POINT('Ctrl Pts',(142.631570420246,-3.0203008691336,340.09022151323));
#11251=CARTESIAN_POINT('Ctrl Pts',(142.624155204218,-2.88397266456738,340.168692917926));
#11252=CARTESIAN_POINT('Ctrl Pts',(142.61673998819,-2.74458903456155,340.241675456747));
#11253=CARTESIAN_POINT('Ctrl Pts',(142.609331907046,-2.60533951878256,340.314587772137));
#11254=CARTESIAN_POINT('Ctrl Pts',(142.601923825902,-2.46304075880642,340.382021563891));
#11255=CARTESIAN_POINT('Ctrl Pts',(142.594515744758,-2.3181645083636,340.443715998715));
#11256=CARTESIAN_POINT('Ctrl Pts',(142.587113177584,-2.17339609195958,340.505364513244));
#11257=CARTESIAN_POINT('Ctrl Pts',(142.57971061041,-2.02605434695135,340.561282031238));
#11258=CARTESIAN_POINT('Ctrl Pts',(142.572308043236,-1.8766345645083,340.611254162288));
#11259=CARTESIAN_POINT('Ctrl Pts',(142.564909373481,-1.7272934509288,340.661199983229));
#11260=CARTESIAN_POINT('Ctrl Pts',(142.557510703726,-1.5758768318851,340.705206533172));
#11261=CARTESIAN_POINT('Ctrl Pts',(142.550112033972,-1.42289875982937,340.743108015855));
#11262=CARTESIAN_POINT('Ctrl Pts',(142.542714584768,-1.26994592440439,340.78100324597));
#11263=CARTESIAN_POINT('Ctrl Pts',(142.535317135564,-1.11543250910901,340.812795318021));
#11264=CARTESIAN_POINT('Ctrl Pts',(142.52791968636,-0.959886584719471,340.838368634043));
#11265=CARTESIAN_POINT('Ctrl Pts',(142.520522557896,-0.804347404530152,
340.86394084125));
#11266=CARTESIAN_POINT('Ctrl Pts',(142.513125429433,-0.647776172527041,
340.883294768003));
#11267=CARTESIAN_POINT('Ctrl Pts',(142.505728300969,-0.490709716235529,
340.896366214618));
#11268=CARTESIAN_POINT('Ctrl Pts',(142.498330033532,-0.333619075630934,
340.90943967391));
#11269=CARTESIAN_POINT('Ctrl Pts',(142.490931766096,-0.17603343085798,340.916228695997));
#11270=CARTESIAN_POINT('Ctrl Pts',(142.483533498659,-0.0184931275726032,
340.916721099286));
#11271=CARTESIAN_POINT('Ctrl Pts',(142.476132632133,0.139102521278442,340.917213675561));
#11272=CARTESIAN_POINT('Ctrl Pts',(142.468731765608,0.296652423953073,340.911405227647));
#11273=CARTESIAN_POINT('Ctrl Pts',(142.461330899082,0.453617990959382,340.899335664359));
#11274=CARTESIAN_POINT('Ctrl Pts',(142.453921905697,0.610755921164594,340.887252847537));
#11275=CARTESIAN_POINT('Ctrl Pts',(142.446512912312,0.767307861944534,340.868895213624));
#11276=CARTESIAN_POINT('Ctrl Pts',(142.439103918928,0.922741358861505,340.844354450848));
#11277=CARTESIAN_POINT('Ctrl Pts',(142.431690361347,1.078270608174,340.819798570115));
#11278=CARTESIAN_POINT('Ctrl Pts',(142.424276803767,1.23267967552981,340.789052043257));
#11279=CARTESIAN_POINT('Ctrl Pts',(142.416863246187,1.38544851873577,340.752257206039));
#11280=CARTESIAN_POINT('Ctrl Pts',(142.40943913405,1.53843485635821,340.715409984635));
#11281=CARTESIAN_POINT('Ctrl Pts',(142.402015021913,1.68977594796262,340.672497356763));
#11282=CARTESIAN_POINT('Ctrl Pts',(142.394590909777,1.83896828253318,340.623711071733));
#11283=CARTESIAN_POINT('Ctrl Pts',(142.390733784622,1.91647970692796,340.598364632491));
#11284=CARTESIAN_POINT('Ctrl Pts',(142.386876659467,1.99341147476138,340.571433552271));
#11285=CARTESIAN_POINT('Ctrl Pts',(142.383019534312,2.06969543560795,340.542949699061));
#11286=CARTESIAN_POINT('Ctrl Pts',(142.375595556874,2.21652251056,340.488125581335));
#11287=CARTESIAN_POINT('Ctrl Pts',(142.368171579436,2.36139122474337,340.427380781077));
#11288=CARTESIAN_POINT('Ctrl Pts',(142.360747601998,2.50378851772458,340.360874333633));
#11289=CARTESIAN_POINT('Ctrl Pts',(142.35333238597,2.6460177604755,340.294446373804));
#11290=CARTESIAN_POINT('Ctrl Pts',(142.345917169943,2.78578105280035,340.222270457918));
#11291=CARTESIAN_POINT('Ctrl Pts',(142.338501953915,2.9225821067375,340.14455482932));
#11292=CARTESIAN_POINT('Ctrl Pts',(142.331093872771,3.05925153138926,340.066913978308));
#11293=CARTESIAN_POINT('Ctrl Pts',(142.323685791627,3.19296406963677,339.983744209301));
#11294=CARTESIAN_POINT('Ctrl Pts',(142.316277710483,3.3232450881857,339.895301078213));
#11295=CARTESIAN_POINT('Ctrl Pts',(142.308875143309,3.45342913619271,339.806923776962));
#11296=CARTESIAN_POINT('Ctrl Pts',(142.301472576135,3.58018644271276,339.71328113772));
#11297=CARTESIAN_POINT('Ctrl Pts',(142.294070008961,3.70306869180658,339.614673642443));
#11298=CARTESIAN_POINT('Ctrl Pts',(142.286671339206,3.82588624393301,339.516118063583));
#11299=CARTESIAN_POINT('Ctrl Pts',(142.279272669451,3.94483251146716,339.412603067566));
#11300=CARTESIAN_POINT('Ctrl Pts',(142.271873999696,4.05948988951751,339.304471210196));
#11301=CARTESIAN_POINT('Ctrl Pts',(142.264476550492,4.17412835266133,339.196357191224));
#11302=CARTESIAN_POINT('Ctrl Pts',(142.257079101288,4.28447905929744,339.083628078318));
#11303=CARTESIAN_POINT('Ctrl Pts',(142.249681652085,4.39015903123336,338.966665380768));
#11304=CARTESIAN_POINT('Ctrl Pts',(142.242284523621,4.49583442106978,338.849707754516));
#11305=CARTESIAN_POINT('Ctrl Pts',(142.234887395158,4.59683922866674,338.728517185517));
#11306=CARTESIAN_POINT('Ctrl Pts',(142.227490266694,4.69282895896306,338.603510361358));
#11307=CARTESIAN_POINT('Ctrl Pts',(142.220091999258,4.78883346928186,338.478484289269));
#11308=CARTESIAN_POINT('Ctrl Pts',(142.212693731821,4.87982113744197,338.349641088041));
#11309=CARTESIAN_POINT('Ctrl Pts',(142.205295464384,4.9654893076409,338.217428553706));
#11310=CARTESIAN_POINT('Ctrl Pts',(142.197894597858,5.05118757396939,338.085169571717));
#11311=CARTESIAN_POINT('Ctrl Pts',(142.190493731333,5.13156241874969,337.949539212921));
#11312=CARTESIAN_POINT('Ctrl Pts',(142.183092864807,5.20635594047811,337.811011985664));
#11313=CARTESIAN_POINT('Ctrl Pts',(142.175683871422,5.28123159264351,337.672332642269));
#11314=CARTESIAN_POINT('Ctrl Pts',(142.168274878037,5.35051350474745,337.530750406306));
#11315=CARTESIAN_POINT('Ctrl Pts',(142.160865884653,5.41399063772855,337.386762647832));
#11316=CARTESIAN_POINT('Ctrl Pts',(142.153452327072,5.47750687481307,337.242686187933));
#11317=CARTESIAN_POINT('Ctrl Pts',(142.146038769492,5.53521107076559,337.096201599101));
#11318=CARTESIAN_POINT('Ctrl Pts',(142.138625211912,5.58694149409885,336.947823221963));
#11319=CARTESIAN_POINT('Ctrl Pts',(142.131201099775,5.63874556516032,336.799233601039));
#11320=CARTESIAN_POINT('Ctrl Pts',(142.123776987638,5.68455876949909,336.64874516312));
#11321=CARTESIAN_POINT('Ctrl Pts',(142.116352875502,5.72426987449761,336.496885087914));
#11322=CARTESIAN_POINT('Ctrl Pts',(142.112495750347,5.74490139233848,336.417987664862));
#11323=CARTESIAN_POINT('Ctrl Pts',(142.108638625193,5.76388666634816,336.338720147219));
#11324=CARTESIAN_POINT('Ctrl Pts',(142.104781500038,5.78121561489331,336.259157089729));
#11325=CARTESIAN_POINT('Ctrl Pts',(142.0973575226,5.81456939986825,336.106018594075));
#11326=CARTESIAN_POINT('Ctrl Pts',(142.089933545162,5.84188457520743,335.951322904724));
#11327=CARTESIAN_POINT('Ctrl Pts',(142.082509567724,5.8630172306863,335.795587528293));
#11328=CARTESIAN_POINT('Ctrl Pts',(142.075094351697,5.88412494645215,335.640035943037));
#11329=CARTESIAN_POINT('Ctrl Pts',(142.067679135669,5.89906461607092,335.483447479264));
#11330=CARTESIAN_POINT('Ctrl Pts',(142.060263919642,5.90774278592052,335.32635216853));
#11331=CARTESIAN_POINT('Ctrl Pts',(142.052855838497,5.91641260567876,335.169408014113));
#11332=CARTESIAN_POINT('Ctrl Pts',(142.045447757353,5.91883289944102,335.01195835378));
#11333=CARTESIAN_POINT('Ctrl Pts',(142.038039676209,5.91496171831772,334.854540612761));
#11334=CARTESIAN_POINT('Ctrl Pts',(142.030637109035,5.91109341858522,334.697240040642));
#11335=CARTESIAN_POINT('Ctrl Pts',(142.023234541861,5.90094297735857,334.539971712033));
#11336=CARTESIAN_POINT('Ctrl Pts',(142.015831974687,5.88452046684895,334.383275233402));
#11337=CARTESIAN_POINT('Ctrl Pts',(142.008433304932,5.86810660271929,334.226661254781));
#11338=CARTESIAN_POINT('Ctrl Pts',(142.001034635178,5.84542728467107,334.070618896769));
#11339=CARTESIAN_POINT('Ctrl Pts',(141.993635965423,5.81654458521853,333.91568470883));
#11340=CARTESIAN_POINT('Ctrl Pts',(141.986238516219,5.78766665051466,333.760776080222));
#11341=CARTESIAN_POINT('Ctrl Pts',(141.978841067015,5.75258743378497,333.606975625394));
#11342=CARTESIAN_POINT('Ctrl Pts',(141.971443617811,5.7114205028552,333.454811855448));
#11343=CARTESIAN_POINT('Ctrl Pts',(141.964046489348,5.67025535685187,333.302654683057));
#11344=CARTESIAN_POINT('Ctrl Pts',(141.956649360884,5.62300311893932,333.152134414708));
#11345=CARTESIAN_POINT('Ctrl Pts',(141.949252232421,5.56982776455352,333.003766237208));
#11346=CARTESIAN_POINT('Ctrl Pts',(141.941853964984,5.51664422249044,332.855375214713));
#11347=CARTESIAN_POINT('Ctrl Pts',(141.934455697547,5.45753587394222,332.709137294216));
#11348=CARTESIAN_POINT('Ctrl Pts',(141.927057430111,5.39271549572256,332.565549313563));
#11349=CARTESIAN_POINT('Ctrl Pts',(141.919656563585,5.32787234542219,332.421910888942));
#11350=CARTESIAN_POINT('Ctrl Pts',(141.912255697059,5.25731332358313,332.280924597633));
#11351=CARTESIAN_POINT('Ctrl Pts',(141.904854830533,5.18129788909323,332.143064098203));
#11352=CARTESIAN_POINT('Ctrl Pts',(141.897445837149,5.10519898238911,332.005052214765));
#11353=CARTESIAN_POINT('Ctrl Pts',(141.890036843764,5.02363187767832,331.870173304945));
#11354=CARTESIAN_POINT('Ctrl Pts',(141.882627850379,4.93690061870751,331.738873991471));
#11355=CARTESIAN_POINT('Ctrl Pts',(141.875214292799,4.85011593028928,331.60749379309));
#11356=CARTESIAN_POINT('Ctrl Pts',(141.867800735219,4.75816096592499,331.479697887347));
#11357=CARTESIAN_POINT('Ctrl Pts',(141.860387177638,4.661380723432,331.355900616927));
#11358=CARTESIAN_POINT('Ctrl Pts',(141.852963065502,4.56446269654597,331.231927098428));
#11359=CARTESIAN_POINT('Ctrl Pts',(141.845538953365,4.46270591219901,331.111963868735));
#11360=CARTESIAN_POINT('Ctrl Pts',(141.838114841228,4.35649349270314,330.996389752919));
#11361=CARTESIAN_POINT('Ctrl Pts',(141.834257716074,4.30131186459401,330.936344346663));
#11362=CARTESIAN_POINT('Ctrl Pts',(141.830400590919,4.24492813904903,330.877483022547));
#11363=CARTESIAN_POINT('Ctrl Pts',(141.826543465765,4.1873995549931,330.819854604282));
#11364=CARTESIAN_POINT('Ctrl Pts',(141.819119488327,4.07667177382124,330.708934667842));
#11365=CARTESIAN_POINT('Ctrl Pts',(141.811695510889,3.96136667707952,330.602250040211));
#11366=CARTESIAN_POINT('Ctrl Pts',(141.804271533451,3.8418415690413,330.500201791093));
#11367=CARTESIAN_POINT('Ctrl Pts',(141.796856317423,3.72245751861409,330.398273974262));
#11368=CARTESIAN_POINT('Ctrl Pts',(141.789441101395,3.59886365122774,330.300971884564));
#11369=CARTESIAN_POINT('Ctrl Pts',(141.782025885368,3.47145510860933,330.208660939632));
#11370=CARTESIAN_POINT('Ctrl Pts',(141.774617804224,3.34416915784892,330.116438815826));
#11371=CARTESIAN_POINT('Ctrl Pts',(141.76720972308,3.21307613926443,330.0291984935));
#11372=CARTESIAN_POINT('Ctrl Pts',(141.759801641936,3.07860528424778,329.947266080002));
#11373=CARTESIAN_POINT('Ctrl Pts',(141.752399074762,2.9442345183446,329.865394650295));
#11374=CARTESIAN_POINT('Ctrl Pts',(141.744996507588,2.80649123946498,329.788823456208));
#11375=CARTESIAN_POINT('Ctrl Pts',(141.737593940414,2.66583466485106,329.717836039824));
#11376=CARTESIAN_POINT('Ctrl Pts',(141.730195270659,2.52525214530864,329.646885998006));
#11377=CARTESIAN_POINT('Ctrl Pts',(141.722796600904,2.38175971710454,329.581514046766));
#11378=CARTESIAN_POINT('Ctrl Pts',(141.71539793115,2.23584216712864,329.521958345705));
#11379=CARTESIAN_POINT('Ctrl Pts',(141.708000481946,2.08994868901739,329.462412469486));
#11380=CARTESIAN_POINT('Ctrl Pts',(141.700603032742,1.94163122834648,329.408681080041));
#11381=CARTESIAN_POINT('Ctrl Pts',(141.693205583538,1.79139567944247,329.360954683444));
#11382=CARTESIAN_POINT('Ctrl Pts',(141.685808455074,1.64116664449027,329.31323035618));
#11383=CARTESIAN_POINT('Ctrl Pts',(141.678411326611,1.48902004235882,329.271510617068));
#11384=CARTESIAN_POINT('Ctrl Pts',(141.671014198147,1.33547784114391,329.235936372808));
#11385=CARTESIAN_POINT('Ctrl Pts',(141.663615930711,1.18191199826283,329.200356651003));
#11386=CARTESIAN_POINT('Ctrl Pts',(141.656217663274,1.02695049203155,329.170924392407));
#11387=CARTESIAN_POINT('Ctrl Pts',(141.648819395838,0.871126269738591,329.147729535926));
#11388=CARTESIAN_POINT('Ctrl Pts',(141.641418529312,0.715247304758272,329.124526530848));
#11389=CARTESIAN_POINT('Ctrl Pts',(141.634017662786,0.558505389193618,329.107565345604));
#11390=CARTESIAN_POINT('Ctrl Pts',(141.626616796261,0.40143924073227,329.096884119509));
#11391=CARTESIAN_POINT('Ctrl Pts',(141.619207802876,0.244200618622956,329.086191164407));
#11392=CARTESIAN_POINT('Ctrl Pts',(141.611798809491,0.0866374251619905,
329.081791965463));
#11393=CARTESIAN_POINT('Ctrl Pts',(141.604389816106,-0.0707102295546171,
329.083672538987));
#11394=CARTESIAN_POINT('Ctrl Pts',(141.596976258526,-0.22815481585403,329.08555427101));
#11395=CARTESIAN_POINT('Ctrl Pts',(141.589562700946,-0.385383226991015,
329.093723464792));
#11396=CARTESIAN_POINT('Ctrl Pts',(141.582149143366,-0.541860335248411,
329.108114228909));
#11397=CARTESIAN_POINT('Ctrl Pts',(141.574725031229,-0.698560217315989,
329.122525480914));
#11398=CARTESIAN_POINT('Ctrl Pts',(141.567300919092,-0.854506291280839,
329.143175944681));
#11399=CARTESIAN_POINT('Ctrl Pts',(141.559876806956,-1.00917266559218,329.169948448468));
#11400=CARTESIAN_POINT('Ctrl Pts',(141.556019681801,-1.08952807402006,329.183857842064));
#11401=CARTESIAN_POINT('Ctrl Pts',(141.552162556646,-1.16953828641434,329.199418879829));
#11402=CARTESIAN_POINT('Ctrl Pts',(141.548305431491,-1.24913127060842,329.216609849639));
#11403=CARTESIAN_POINT('Ctrl Pts',(141.540881454053,-1.40232736748535,329.249698060908));
#11404=CARTESIAN_POINT('Ctrl Pts',(141.533457476615,-1.55443895092883,329.288927403111));
#11405=CARTESIAN_POINT('Ctrl Pts',(141.526033499177,-1.70493539502551,329.334214453292));
#11406=CARTESIAN_POINT('Ctrl Pts',(141.51861828315,-1.85525423067496,329.379448057939));
#11407=CARTESIAN_POINT('Ctrl Pts',(141.511203067122,-2.00396136720902,329.430725033856));
#11408=CARTESIAN_POINT('Ctrl Pts',(141.503787851094,-2.15053568328211,329.487910846382));
#11409=CARTESIAN_POINT('Ctrl Pts',(141.49637976995,-2.29696896628602,329.545041635008));
#11410=CARTESIAN_POINT('Ctrl Pts',(141.488971688806,-2.4412731689922,329.608069806823));
#11411=CARTESIAN_POINT('Ctrl Pts',(141.481563607662,-2.58294177904009,329.676810887392));
#11412=CARTESIAN_POINT('Ctrl Pts',(141.474161040488,-2.72450494255493,329.745500802719));
#11413=CARTESIAN_POINT('Ctrl Pts',(141.466758473314,-2.8634360851482,329.819894997779));
#11414=CARTESIAN_POINT('Ctrl Pts',(141.45935590614,-2.99924826143191,329.899760747887));
#11415=CARTESIAN_POINT('Ctrl Pts',(141.451957236385,-3.13498893319731,329.979584449026));
#11416=CARTESIAN_POINT('Ctrl Pts',(141.44455856663,-3.26761358813892,330.064873779321));
#11417=CARTESIAN_POINT('Ctrl Pts',(141.437159896875,-3.39665960676462,330.155349952961));
#11418=CARTESIAN_POINT('Ctrl Pts',(141.429762447671,-3.5256843368049,330.245811200842));
#11419=CARTESIAN_POINT('Ctrl Pts',(141.422364998467,-3.65113129692158,330.341457379799));
#11420=CARTESIAN_POINT('Ctrl Pts',(141.414967549263,-3.77256651804377,330.441966166269));
#11421=CARTESIAN_POINT('Ctrl Pts',(141.4075704208,-3.89399647394623,330.542470594853));
#11422=CARTESIAN_POINT('Ctrl Pts',(141.400173292336,-4.01141474920077,330.647836973779));
#11423=CARTESIAN_POINT('Ctrl Pts',(141.392776163873,-4.12442038546909,330.757702621642));
#11424=CARTESIAN_POINT('Ctrl Pts',(141.385377896436,-4.2374434217844,330.867585186071));
#11425=CARTESIAN_POINT('Ctrl Pts',(141.377979628999,-4.34605219865847,330.981968138671));
#11426=CARTESIAN_POINT('Ctrl Pts',(141.370581361563,-4.44988267618832,331.100451983799));
#11427=CARTESIAN_POINT('Ctrl Pts',(141.363180495037,-4.55374963045635,331.218977453547));
#11428=CARTESIAN_POINT('Ctrl Pts',(141.355779628511,-4.65283469734034,331.341606403719));
#11429=CARTESIAN_POINT('Ctrl Pts',(141.348378761986,-4.74681427362334,331.467906454491));
#11430=CARTESIAN_POINT('Ctrl Pts',(141.340969768601,-4.84089704846656,331.594345194794));
#11431=CARTESIAN_POINT('Ctrl Pts',(141.333560775216,-4.92986291366767,331.724462786665));
#11432=CARTESIAN_POINT('Ctrl Pts',(141.326151781831,-5.01343134384435,331.857797472622));
#11433=CARTESIAN_POINT('Ctrl Pts',(141.318738224251,-5.09705125505637,331.991214297345));
#11434=CARTESIAN_POINT('Ctrl Pts',(141.311324666671,-5.17526692075334,332.127851842095));
#11435=CARTESIAN_POINT('Ctrl Pts',(141.30391110909,-5.24784416212585,332.267224448927));
#11436=CARTESIAN_POINT('Ctrl Pts',(141.296486996954,-5.3205247304886,332.406795478181));
#11437=CARTESIAN_POINT('Ctrl Pts',(141.289062884817,-5.38755068375463,332.54910900961));
#11438=CARTESIAN_POINT('Ctrl Pts',(141.28163877268,-5.44873596404843,332.693659401436));
#11439=CARTESIAN_POINT('Ctrl Pts',(141.277781647526,-5.48052418052112,332.768759149684));
#11440=CARTESIAN_POINT('Ctrl Pts',(141.273924522371,-5.51073668879568,332.844462414655));
#11441=CARTESIAN_POINT('Ctrl Pts',(141.270067397216,-5.53935276631987,332.920696873286));
#11442=CARTESIAN_POINT('Ctrl Pts',(141.261553144537,-5.60252015264225,333.088977501382));
#11443=CARTESIAN_POINT('Ctrl Pts',(141.253038891857,-5.65806380752951,333.260267546807));
#11444=CARTESIAN_POINT('Ctrl Pts',(141.244524639177,-5.70572547026194,333.433913341956));
#11445=CARTESIAN_POINT('Ctrl Pts',(141.23603957969,-5.75322371335498,333.606963750129));
#11446=CARTESIAN_POINT('Ctrl Pts',(141.227554520203,-5.79289382508951,333.782353644897));
#11447=CARTESIAN_POINT('Ctrl Pts',(141.219069460716,-5.82452667773354,333.959413846493));
#11448=CARTESIAN_POINT('Ctrl Pts',(141.210642121583,-5.85594434515345,334.135269580709));
#11449=CARTESIAN_POINT('Ctrl Pts',(141.202214782449,-5.87943365279655,334.312772823345));
#11450=CARTESIAN_POINT('Ctrl Pts',(141.193787443315,-5.89483690462232,334.491248164227));
#11451=CARTESIAN_POINT('Ctrl Pts',(141.18587565336,-5.90929785025902,334.658805134091));
#11452=CARTESIAN_POINT('Ctrl Pts',(141.177963863405,-5.91663213484256,334.827218636702));
#11453=CARTESIAN_POINT('Ctrl Pts',(141.170052073449,-5.91674859019896,334.995915532029));
#11454=CARTESIAN_POINT('',(139.420051969975,-5.91362844489661,335.004262364622));
#11455=CARTESIAN_POINT('Ctrl Pts',(141.170052004703,-5.91002799473302,334.995921635567));
#11456=CARTESIAN_POINT('Ctrl Pts',(141.11064445745,-5.90202012525986,336.261189543943));
#11457=CARTESIAN_POINT('Ctrl Pts',(140.958490898771,-4.88291250323578,339.513541639599));
#11458=CARTESIAN_POINT('Ctrl Pts',(140.71359132867,0.475935523755951,341.980408891924));
#11459=CARTESIAN_POINT('Ctrl Pts',(140.435353294395,6.12753077878764,338.377275451633));
#11460=CARTESIAN_POINT('Ctrl Pts',(140.157115260122,6.15598148033646,331.674866177885));
#11461=CARTESIAN_POINT('Ctrl Pts',(139.878877225847,0.535178839515167,328.023883133794));
#11462=CARTESIAN_POINT('Ctrl Pts',(139.633189474041,-4.86173227124819,330.452959959149));
#11463=CARTESIAN_POINT('Ctrl Pts',(139.48024773366,-5.90188289997479,333.722401776941));
#11464=CARTESIAN_POINT('Ctrl Pts',(139.420052004703,-5.91038989499448,335.004259290461));
#11465=CARTESIAN_POINT('',(137.670052004703,-5.92107572873037,335.002186220721));
#11466=CARTESIAN_POINT('Ctrl Pts',(139.420051936518,-5.91674846258414,335.004265326268));
#11467=CARTESIAN_POINT('Ctrl Pts',(139.4115646907,-5.91661803343069,335.185193218922));
#11468=CARTESIAN_POINT('Ctrl Pts',(139.403077444883,-5.90818479430956,335.365788285949));
#11469=CARTESIAN_POINT('Ctrl Pts',(139.394590199065,-5.89156394627951,335.545348356007));
#11470=CARTESIAN_POINT('Ctrl Pts',(139.386063051631,-5.87486495762325,335.725752602986));
#11471=CARTESIAN_POINT('Ctrl Pts',(139.377535904197,-5.84990129915733,335.905111962886));
#11472=CARTESIAN_POINT('Ctrl Pts',(139.369008756763,-5.81683933887567,336.082732962557));
#11473=CARTESIAN_POINT('Ctrl Pts',(139.36042855897,-5.78357168860522,336.261459004432));
#11474=CARTESIAN_POINT('Ctrl Pts',(139.351848361177,-5.74210474159252,336.438424854248));
#11475=CARTESIAN_POINT('Ctrl Pts',(139.343268163383,-5.69265661404864,336.612944895844));
#11476=CARTESIAN_POINT('Ctrl Pts',(139.336312494689,-5.65257073245615,336.754422239283));
#11477=CARTESIAN_POINT('Ctrl Pts',(139.329356825994,-5.60724073314045,336.894292621023));
#11478=CARTESIAN_POINT('Ctrl Pts',(139.322401157299,-5.55680547474913,337.032201633278));
#11479=CARTESIAN_POINT('Ctrl Pts',(139.314977179861,-5.50297452954355,337.179395733574));
#11480=CARTESIAN_POINT('Ctrl Pts',(139.307553202423,-5.44320980679537,337.324671516216));
#11481=CARTESIAN_POINT('Ctrl Pts',(139.300129224985,-5.37766687213299,337.467514858084));
#11482=CARTESIAN_POINT('Ctrl Pts',(139.292714008957,-5.31220128799499,337.610189623316));
#11483=CARTESIAN_POINT('Ctrl Pts',(139.28529879293,-5.24097121971824,337.750437325931));
#11484=CARTESIAN_POINT('Ctrl Pts',(139.277883576902,-5.16418155311644,337.88776028246));
#11485=CARTESIAN_POINT('Ctrl Pts',(139.270475495758,-5.08746577314524,338.024951107532));
#11486=CARTESIAN_POINT('Ctrl Pts',(139.263067414614,-5.00520122547612,338.159222465453));
#11487=CARTESIAN_POINT('Ctrl Pts',(139.25565933347,-4.9176402537058,338.290098007299));
#11488=CARTESIAN_POINT('Ctrl Pts',(139.248256766296,-4.83014445516577,338.420876136089));
#11489=CARTESIAN_POINT('Ctrl Pts',(139.240854199122,-4.73736028870984,338.548263172698));
#11490=CARTESIAN_POINT('Ctrl Pts',(139.233451631948,-4.63958520074719,338.671808781446));
#11491=CARTESIAN_POINT('Ctrl Pts',(139.226052962193,-4.54186159094163,338.795289343972));
#11492=CARTESIAN_POINT('Ctrl Pts',(139.218654292438,-4.43915252387025,338.914932214641));
#11493=CARTESIAN_POINT('Ctrl Pts',(139.211255622683,-4.33179772630097,339.030317483886));
#11494=CARTESIAN_POINT('Ctrl Pts',(139.203858173479,-4.22446063893921,339.145683718144));
#11495=CARTESIAN_POINT('Ctrl Pts',(139.196460724275,-4.11247959611186,339.256793471987));
#11496=CARTESIAN_POINT('Ctrl Pts',(139.189063275071,-3.99623351111238,339.363261198595));
#11497=CARTESIAN_POINT('Ctrl Pts',(139.181666146608,-3.87999246634052,339.469724308947));
#11498=CARTESIAN_POINT('Ctrl Pts',(139.174269018144,-3.7594870223097,339.571545540186));
#11499=CARTESIAN_POINT('Ctrl Pts',(139.166871889681,-3.63513152978765,339.668377590089));
#11500=CARTESIAN_POINT('Ctrl Pts',(139.159473622244,-3.51075688962381,339.76522454971));
#11501=CARTESIAN_POINT('Ctrl Pts',(139.152075354808,-3.38253131508879,339.857080569083));
#11502=CARTESIAN_POINT('Ctrl Pts',(139.144677087371,-3.25090054733828,339.94363997413));
#11503=CARTESIAN_POINT('Ctrl Pts',(139.137276220845,-3.1192235363147,340.030229788406));
#11504=CARTESIAN_POINT('Ctrl Pts',(139.129875354319,-2.9841392619177,340.111519078666));
#11505=CARTESIAN_POINT('Ctrl Pts',(139.122474487794,-2.84612047935495,340.187246743649));
#11506=CARTESIAN_POINT('Ctrl Pts',(139.115065494409,-2.70795013897403,340.263057564848));
#11507=CARTESIAN_POINT('Ctrl Pts',(139.107656501024,-2.56683918257287,340.333294384741));
#11508=CARTESIAN_POINT('Ctrl Pts',(139.100247507639,-2.42328354313969,340.397742808994));
#11509=CARTESIAN_POINT('Ctrl Pts',(139.092833950059,-2.27963946848091,340.4622309357));
#11510=CARTESIAN_POINT('Ctrl Pts',(139.085420392479,-2.13354805536722,340.52092342253));
#11511=CARTESIAN_POINT('Ctrl Pts',(139.078006834899,-1.98552254007584,340.573655066951));
#11512=CARTESIAN_POINT('Ctrl Pts',(139.070582722762,-1.83728628336381,340.626461784522));
#11513=CARTESIAN_POINT('Ctrl Pts',(139.063158610625,-1.68711078041681,340.673290599943));
#11514=CARTESIAN_POINT('Ctrl Pts',(139.055734498488,-1.53552244745772,340.714026721661));
#11515=CARTESIAN_POINT('Ctrl Pts',(139.051877373334,-1.45676620544673,340.735190776954));
#11516=CARTESIAN_POINT('Ctrl Pts',(139.04802024818,-1.37762875574112,340.754711126236));
#11517=CARTESIAN_POINT('Ctrl Pts',(139.044163123025,-1.29818458327537,340.772577184434));
#11518=CARTESIAN_POINT('Ctrl Pts',(139.036739145587,-1.14527491081934,340.806964767843));
#11519=CARTESIAN_POINT('Ctrl Pts',(139.029315168149,-0.990767285094664,
340.83532439937));
#11520=CARTESIAN_POINT('Ctrl Pts',(139.021891190711,-0.835178228691196,
340.857508675949));
#11521=CARTESIAN_POINT('Ctrl Pts',(139.014475974684,-0.679772790783808,
340.879666771744));
#11522=CARTESIAN_POINT('Ctrl Pts',(139.007060758656,-0.523288828476869,
340.895663967));
#11523=CARTESIAN_POINT('Ctrl Pts',(138.999645542629,-0.366255729886668,
340.905403229486));
#11524=CARTESIAN_POINT('Ctrl Pts',(138.992237461484,-0.209373727753261,
340.915133120903));
#11525=CARTESIAN_POINT('Ctrl Pts',(138.98482938034,-0.0519440112410602,
340.918617043992));
#11526=CARTESIAN_POINT('Ctrl Pts',(138.977421299196,0.105496290076524,340.915809420128));
#11527=CARTESIAN_POINT('Ctrl Pts',(138.970018732022,0.262819405702351,340.913003886031));
#11528=CARTESIAN_POINT('Ctrl Pts',(138.962616164848,0.42015271889278,340.903916135971));
#11529=CARTESIAN_POINT('Ctrl Pts',(138.955213597674,0.576956567449006,340.888552596503));
#11530=CARTESIAN_POINT('Ctrl Pts',(138.947814927919,0.733677859464217,340.873197145871));
#11531=CARTESIAN_POINT('Ctrl Pts',(138.940416258165,0.889869871516724,340.851572522595));
#11532=CARTESIAN_POINT('Ctrl Pts',(138.93301758841,1.04499564704305,340.823737172998));
#11533=CARTESIAN_POINT('Ctrl Pts',(138.925620139206,1.20009583163343,340.79590641537));
#11534=CARTESIAN_POINT('Ctrl Pts',(138.918222690002,1.35412976180707,340.761867030727));
#11535=CARTESIAN_POINT('Ctrl Pts',(138.910825240798,1.5065681712928,340.721729013834));
#11536=CARTESIAN_POINT('Ctrl Pts',(138.903428112334,1.6589999713148,340.681592737255));
#11537=CARTESIAN_POINT('Ctrl Pts',(138.896030983871,1.80983602728958,340.635358449223));
#11538=CARTESIAN_POINT('Ctrl Pts',(138.888633855407,1.95856005639423,340.583186640978));
#11539=CARTESIAN_POINT('Ctrl Pts',(138.881235587971,2.10730698528692,340.531006799577));
#11540=CARTESIAN_POINT('Ctrl Pts',(138.873837320534,2.25394088760211,340.472887741158));
#11541=CARTESIAN_POINT('Ctrl Pts',(138.866439053098,2.39796349937133,340.409038881186));
#11542=CARTESIAN_POINT('Ctrl Pts',(138.859038186572,2.54203670779859,340.345167590438));
#11543=CARTESIAN_POINT('Ctrl Pts',(138.851637320046,2.68349645821875,340.27556264154));
#11544=CARTESIAN_POINT('Ctrl Pts',(138.84423645352,2.82186735004229,340.200480287557));
#11545=CARTESIAN_POINT('Ctrl Pts',(138.836827460135,2.96039018633387,340.125315485971));
#11546=CARTESIAN_POINT('Ctrl Pts',(138.829418466751,3.09581706207243,340.044661445695));
#11547=CARTESIAN_POINT('Ctrl Pts',(138.822009473366,3.2276993106918,339.958819186284));
#11548=CARTESIAN_POINT('Ctrl Pts',(138.814595915786,3.35966280332542,339.87292404508));
#11549=CARTESIAN_POINT('Ctrl Pts',(138.807182358205,3.4880770140096,339.781834531468));
#11550=CARTESIAN_POINT('Ctrl Pts',(138.799768800625,3.61252527881023,339.685892836211));
#11551=CARTESIAN_POINT('Ctrl Pts',(138.792344688488,3.73715071849896,339.589814550387));
#11552=CARTESIAN_POINT('Ctrl Pts',(138.784920576352,3.85779865014862,339.488870525167));
#11553=CARTESIAN_POINT('Ctrl Pts',(138.777496464215,3.9740876690689,339.383441314887));
#11554=CARTESIAN_POINT('Ctrl Pts',(138.77363933906,4.0345044962691,339.328666595498));
#11555=CARTESIAN_POINT('Ctrl Pts',(138.769782213906,4.09374538937467,339.272681806787));
#11556=CARTESIAN_POINT('Ctrl Pts',(138.765925088751,4.15176113909933,339.215543856534));
#11557=CARTESIAN_POINT('Ctrl Pts',(138.758501111313,4.26342658933596,339.105567945323));
#11558=CARTESIAN_POINT('Ctrl Pts',(138.751077133875,4.37088775043844,338.990986210471));
#11559=CARTESIAN_POINT('Ctrl Pts',(138.743653156437,4.47374114801233,338.872153238585));
#11560=CARTESIAN_POINT('Ctrl Pts',(138.73623794041,4.57647316310195,338.753460507485));
#11561=CARTESIAN_POINT('Ctrl Pts',(138.728822724382,4.67460799692951,338.630526805414));
#11562=CARTESIAN_POINT('Ctrl Pts',(138.721407508354,4.76777757073667,338.503744796426));
#11563=CARTESIAN_POINT('Ctrl Pts',(138.71399942721,4.86085749724903,338.377084776448));
#11564=CARTESIAN_POINT('Ctrl Pts',(138.706591346066,4.94898145541993,338.246584119908));
#11565=CARTESIAN_POINT('Ctrl Pts',(138.699183264922,5.03182044558077,338.112669845315));
#11566=CARTESIAN_POINT('Ctrl Pts',(138.691780697748,5.11459777716832,337.978855245563));
#11567=CARTESIAN_POINT('Ctrl Pts',(138.684378130574,5.19209777781471,337.841632402929));
#11568=CARTESIAN_POINT('Ctrl Pts',(138.6769755634,5.26403380956595,337.701458608649));
#11569=CARTESIAN_POINT('Ctrl Pts',(138.669576893645,5.33593196731082,337.56135861526));
#11570=CARTESIAN_POINT('Ctrl Pts',(138.662178223891,5.40227182027408,337.418311095639));
#11571=CARTESIAN_POINT('Ctrl Pts',(138.654779554136,5.46281193920951,337.272799216678));
#11572=CARTESIAN_POINT('Ctrl Pts',(138.647382104932,5.52334207090526,337.127311342657));
#11573=CARTESIAN_POINT('Ctrl Pts',(138.639984655728,5.57807422424232,336.979360260395));
#11574=CARTESIAN_POINT('Ctrl Pts',(138.632587206524,5.6268144798169,336.829450565668));
#11575=CARTESIAN_POINT('Ctrl Pts',(138.625190078061,5.67555262209895,336.679547370764));
#11576=CARTESIAN_POINT('Ctrl Pts',(138.617792949597,5.71829926778662,336.527686087172));
#11577=CARTESIAN_POINT('Ctrl Pts',(138.610395821134,5.75490998712807,336.374387719151));
#11578=CARTESIAN_POINT('Ctrl Pts',(138.602997553697,5.79152634360639,336.221065747008));
#11579=CARTESIAN_POINT('Ctrl Pts',(138.59559928626,5.82200480586053,336.066306612873));
#11580=CARTESIAN_POINT('Ctrl Pts',(138.588201018824,5.84625183659871,335.910642644272));
#11581=CARTESIAN_POINT('Ctrl Pts',(138.580800152298,5.87050738557378,335.754923989281));
#11582=CARTESIAN_POINT('Ctrl Pts',(138.573399285772,5.8885270869998,335.598300235461));
#11583=CARTESIAN_POINT('Ctrl Pts',(138.565998419247,5.9002691630095,335.441309830549));
#11584=CARTESIAN_POINT('Ctrl Pts',(138.558589425862,5.91202413294125,335.284147035163));
#11585=CARTESIAN_POINT('Ctrl Pts',(138.551180432477,5.91748768304993,335.126617157028));
#11586=CARTESIAN_POINT('Ctrl Pts',(138.543771439092,5.91667014787691,334.969260388385));
#11587=CARTESIAN_POINT('Ctrl Pts',(138.536357881512,5.91585210907402,334.811806682545));
#11588=CARTESIAN_POINT('Ctrl Pts',(138.528944323932,5.90874529157503,334.654526670653));
#11589=CARTESIAN_POINT('Ctrl Pts',(138.521530766352,5.89541197013135,334.497955913358));
#11590=CARTESIAN_POINT('Ctrl Pts',(138.514106654215,5.88205966626361,334.341162248927));
#11591=CARTESIAN_POINT('Ctrl Pts',(138.506682542078,5.86246320050229,334.185080225078));
#11592=CARTESIAN_POINT('Ctrl Pts',(138.499258429942,5.83673618914445,334.030236512942));
#11593=CARTESIAN_POINT('Ctrl Pts',(138.495401304787,5.82336997095747,333.949788970376));
#11594=CARTESIAN_POINT('Ctrl Pts',(138.491544179632,5.80834981424833,333.869675457934));
#11595=CARTESIAN_POINT('Ctrl Pts',(138.487687054477,5.79169694401467,333.789968152819));
#11596=CARTESIAN_POINT('Ctrl Pts',(138.480263077039,5.75964443652942,333.636552017465));
#11597=CARTESIAN_POINT('Ctrl Pts',(138.472839099601,5.72144361159046,333.484178883083));
#11598=CARTESIAN_POINT('Ctrl Pts',(138.465415122163,5.67717430549523,333.333379927061));
#11599=CARTESIAN_POINT('Ctrl Pts',(138.457999906136,5.63295724384186,333.182758936495));
#11600=CARTESIAN_POINT('Ctrl Pts',(138.450584690108,5.58268606065472,333.033708780989));
#11601=CARTESIAN_POINT('Ctrl Pts',(138.443169474081,5.52649176697713,332.886751478876));
#11602=CARTESIAN_POINT('Ctrl Pts',(138.435761392936,5.47035154316597,332.739935578338));
#11603=CARTESIAN_POINT('Ctrl Pts',(138.428353311792,5.4082996872901,332.59520886849));
#11604=CARTESIAN_POINT('Ctrl Pts',(138.420945230648,5.34051724772555,332.45307909639));
#11605=CARTESIAN_POINT('Ctrl Pts',(138.413542663474,5.27278525986872,332.311055114075));
#11606=CARTESIAN_POINT('Ctrl Pts',(138.4061400963,5.19933134127639,332.171624556147));
#11607=CARTESIAN_POINT('Ctrl Pts',(138.398737529126,5.120384921659,332.035275929105));
#11608=CARTESIAN_POINT('Ctrl Pts',(138.391338859372,5.04148006698646,331.898999089018));
#11609=CARTESIAN_POINT('Ctrl Pts',(138.383940189617,4.95708865697102,331.76580127043));
#11610=CARTESIAN_POINT('Ctrl Pts',(138.376541519862,4.8674863457395,331.636146965675));
#11611=CARTESIAN_POINT('Ctrl Pts',(138.369144070658,4.77789881610706,331.506514049853));
#11612=CARTESIAN_POINT('Ctrl Pts',(138.361746621454,4.68310230333574,331.380423794409));
#11613=CARTESIAN_POINT('Ctrl Pts',(138.35434917225,4.58341619186373,331.258312336036));
#11614=CARTESIAN_POINT('Ctrl Pts',(138.346952043787,4.48373440260772,331.136206172202));
#11615=CARTESIAN_POINT('Ctrl Pts',(138.339554915323,4.37916367220048,331.018078751534));
#11616=CARTESIAN_POINT('Ctrl Pts',(138.33215778686,4.27006396501272,330.904333473389));
#11617=CARTESIAN_POINT('Ctrl Pts',(138.324759519423,4.1609474591935,330.790570681311));
#11618=CARTESIAN_POINT('Ctrl Pts',(138.317361251987,4.04730084643777,330.681191644615));
#11619=CARTESIAN_POINT('Ctrl Pts',(138.30996298455,3.9295211539225,330.576563093773));
#11620=CARTESIAN_POINT('Ctrl Pts',(138.302562118024,3.8117000841626,330.47189778582));
#11621=CARTESIAN_POINT('Ctrl Pts',(138.295161251498,3.68974332256651,330.371986534196));
#11622=CARTESIAN_POINT('Ctrl Pts',(138.287760384973,3.56408105292134,330.277155855768));
#11623=CARTESIAN_POINT('Ctrl Pts',(138.280351391588,3.43828079409031,330.182221044188));
#11624=CARTESIAN_POINT('Ctrl Pts',(138.272942398203,3.30876719927659,330.092378172221));
#11625=CARTESIAN_POINT('Ctrl Pts',(138.265533404818,3.17600012027299,330.007910878347));
#11626=CARTESIAN_POINT('Ctrl Pts',(138.258119847238,3.04315125216899,329.923391549706));
#11627=CARTESIAN_POINT('Ctrl Pts',(138.250706289658,2.90704522800942,329.844254584999));
#11628=CARTESIAN_POINT('Ctrl Pts',(138.243292732078,2.76816611261098,329.770737438654));
#11629=CARTESIAN_POINT('Ctrl Pts',(138.235868619941,2.6290892773668,329.697115627193));
#11630=CARTESIAN_POINT('Ctrl Pts',(138.228444507804,2.48723180158059,329.629129774235));
#11631=CARTESIAN_POINT('Ctrl Pts',(138.221020395668,2.34309805853791,329.56696934938));
#11632=CARTESIAN_POINT('Ctrl Pts',(138.217163270513,2.26821477610547,329.534674506047));
#11633=CARTESIAN_POINT('Ctrl Pts',(138.213306145358,2.19271734569308,329.50395125777));
#11634=CARTESIAN_POINT('Ctrl Pts',(138.209449020203,2.11667794871525,329.47482081522));
#11635=CARTESIAN_POINT('Ctrl Pts',(138.202025042765,1.97032159653299,329.418752178719));
#11636=CARTESIAN_POINT('Ctrl Pts',(138.194601065327,1.82151511875569,329.368418221206));
#11637=CARTESIAN_POINT('Ctrl Pts',(138.187177087889,1.67074839778092,329.3240392572));
#11638=CARTESIAN_POINT('Ctrl Pts',(138.179761871862,1.52015960422103,329.279712667048));
#11639=CARTESIAN_POINT('Ctrl Pts',(138.172346655834,1.36761552682853,329.241327185838));
#11640=CARTESIAN_POINT('Ctrl Pts',(138.164931439806,1.21362603954763,329.209055137663));
#11641=CARTESIAN_POINT('Ctrl Pts',(138.157523358662,1.05978472017605,329.176814141489));
#11642=CARTESIAN_POINT('Ctrl Pts',(138.150115277518,0.904501122506735,329.150674943798));
#11643=CARTESIAN_POINT('Ctrl Pts',(138.142707196374,0.74830019753795,329.130760068215));
#11644=CARTESIAN_POINT('Ctrl Pts',(138.1353046292,0.592215535770415,329.110860015637));
#11645=CARTESIAN_POINT('Ctrl Pts',(138.127902062026,0.43521527485345,329.097175107434));
#11646=CARTESIAN_POINT('Ctrl Pts',(138.120499494852,0.277834367903025,329.089776770162));
#11647=CARTESIAN_POINT('Ctrl Pts',(138.113100825097,0.120536321312057,329.082382328083));
#11648=CARTESIAN_POINT('Ctrl Pts',(138.105702155343,-0.0371416003263249,
329.08126788265));
#11649=CARTESIAN_POINT('Ctrl Pts',(138.098303485588,-0.19465962323581,329.086452993881));
#11650=CARTESIAN_POINT('Ctrl Pts',(138.090906036384,-0.352151660562655,
329.091637249729));
#11651=CARTESIAN_POINT('Ctrl Pts',(138.08350858718,-0.509483478866495,329.103118987435));
#11652=CARTESIAN_POINT('Ctrl Pts',(138.076111137976,-0.666115484251976,
329.120865648402));
#11653=CARTESIAN_POINT('Ctrl Pts',(138.068714009513,-0.822740698346717,
329.138611539905));
#11654=CARTESIAN_POINT('Ctrl Pts',(138.061316881049,-0.978665789015709,
329.162621772549));
#11655=CARTESIAN_POINT('Ctrl Pts',(138.053919752586,-1.13335673175562,329.192811947157));
#11656=CARTESIAN_POINT('Ctrl Pts',(138.046521485149,-1.28807149303932,329.223006770298));
#11657=CARTESIAN_POINT('Ctrl Pts',(138.039123217712,-1.4415513617005,329.259383358584));
#11658=CARTESIAN_POINT('Ctrl Pts',(138.031724950276,-1.59327309207363,329.301806302294));
#11659=CARTESIAN_POINT('Ctrl Pts',(138.02432408375,-1.74504812388613,329.34424414963));
#11660=CARTESIAN_POINT('Ctrl Pts',(138.016923217224,-1.89506342846661,329.39273248113));
#11661=CARTESIAN_POINT('Ctrl Pts',(138.009522350698,-2.04281163368548,329.447086243081));
#11662=CARTESIAN_POINT('Ctrl Pts',(138.002113357314,-2.19072208055903,329.501499690659));
#11663=CARTESIAN_POINT('Ctrl Pts',(137.994704363929,-2.33636010595233,329.561791302385));
#11664=CARTESIAN_POINT('Ctrl Pts',(137.987295370544,-2.47923834002398,329.627727872133));
#11665=CARTESIAN_POINT('Ctrl Pts',(137.979881812964,-2.62220459201622,329.693705061083));
#11666=CARTESIAN_POINT('Ctrl Pts',(137.972468255384,-2.76240733338685,329.765333968012));
#11667=CARTESIAN_POINT('Ctrl Pts',(137.965054697803,-2.89938492839136,329.842336032707));
#11668=CARTESIAN_POINT('Ctrl Pts',(137.957630585667,-3.03655753607932,329.919447723937));
#11669=CARTESIAN_POINT('Ctrl Pts',(137.95020647353,-3.17049551017452,330.00194765566));
#11670=CARTESIAN_POINT('Ctrl Pts',(137.942782361393,-3.30076657632252,330.08951422249));
#11671=CARTESIAN_POINT('Ctrl Pts',(137.938925236239,-3.36844763998588,330.135008579446));
#11672=CARTESIAN_POINT('Ctrl Pts',(137.935068111084,-3.43513946655055,330.181869866803));
#11673=CARTESIAN_POINT('Ctrl Pts',(137.931210985929,-3.50078515800388,330.230048863982));
#11674=CARTESIAN_POINT('Ctrl Pts',(137.923853689573,-3.62600142327591,330.321948179196));
#11675=CARTESIAN_POINT('Ctrl Pts',(137.916496393216,-3.74780208890084,330.418932458763));
#11676=CARTESIAN_POINT('Ctrl Pts',(137.90913909686,-3.86574122611928,330.520717095876));
#11677=CARTESIAN_POINT('Ctrl Pts',(137.901790515492,-3.9835406600795,330.622381165331));
#11678=CARTESIAN_POINT('Ctrl Pts',(137.894441934124,-4.09748738239249,330.728834031429));
#11679=CARTESIAN_POINT('Ctrl Pts',(137.887093352756,-4.20716463146982,330.839748045345));
#11680=CARTESIAN_POINT('Ctrl Pts',(137.879751801412,-4.31673695776895,330.950555953332));
#11681=CARTESIAN_POINT('Ctrl Pts',(137.872410250067,-4.42204767382149,331.065816246674));
#11682=CARTESIAN_POINT('Ctrl Pts',(137.865068698722,-4.52271347061143,331.185161415571));
#11683=CARTESIAN_POINT('Ctrl Pts',(137.857732498819,-4.62330588956094,331.304419590761));
#11684=CARTESIAN_POINT('Ctrl Pts',(137.850396298917,-4.71925988458935,331.427756424704));
#11685=CARTESIAN_POINT('Ctrl Pts',(137.843060099014,-4.81022952951789,331.554768159346));
#11686=CARTESIAN_POINT('Ctrl Pts',(137.835727033594,-4.90116030653324,331.681725626644));
#11687=CARTESIAN_POINT('Ctrl Pts',(137.828393968174,-4.98711074909594,331.81235456212));
#11688=CARTESIAN_POINT('Ctrl Pts',(137.821060902754,-5.06777577911225,331.946218865874));
#11689=CARTESIAN_POINT('Ctrl Pts',(137.81372937577,-5.14842388606251,332.080055085656));
#11690=CARTESIAN_POINT('Ctrl Pts',(137.806397848785,-5.2237885900084,332.217124997622));
#11691=CARTESIAN_POINT('Ctrl Pts',(137.799066321801,-5.2936087853043,332.356964512034));
#11692=CARTESIAN_POINT('Ctrl Pts',(137.791734821713,-5.363428724454,332.496803513422));
#11693=CARTESIAN_POINT('Ctrl Pts',(137.784403321626,-5.42770402531529,332.639411756516));
#11694=CARTESIAN_POINT('Ctrl Pts',(137.777071821538,-5.4862202114806,332.78430183607));
#11695=CARTESIAN_POINT('Ctrl Pts',(137.769738837051,-5.54474824534539,332.929221251338));
#11696=CARTESIAN_POINT('Ctrl Pts',(137.762405852564,-5.5975147017393,333.076423069507));
#11697=CARTESIAN_POINT('Ctrl Pts',(137.755072868076,-5.64435388013823,333.225401499418));
#11698=CARTESIAN_POINT('Ctrl Pts',(137.747732768696,-5.69123850466704,333.374524476977));
#11699=CARTESIAN_POINT('Ctrl Pts',(137.740392669315,-5.7321842498568,333.525427145767));
#11700=CARTESIAN_POINT('Ctrl Pts',(137.733052569934,-5.76707562313242,333.677589579755));
#11701=CARTESIAN_POINT('Ctrl Pts',(137.725708798612,-5.80198445108681,333.829828134175));
#11702=CARTESIAN_POINT('Ctrl Pts',(137.71836502729,-5.83083280290243,333.983327335639));
#11703=CARTESIAN_POINT('Ctrl Pts',(137.711021255968,-5.85355676798457,334.137559435971));
#11704=CARTESIAN_POINT('Ctrl Pts',(137.703666819554,-5.87631373425489,334.292015521975));
#11705=CARTESIAN_POINT('Ctrl Pts',(137.696312383139,-5.89292850420375,334.447206255056));
#11706=CARTESIAN_POINT('Ctrl Pts',(137.688957946725,-5.9033891956881,334.602600243164));
#11707=CARTESIAN_POINT('Ctrl Pts',(137.682655966051,-5.91235291117344,334.735756593261));
#11708=CARTESIAN_POINT('Ctrl Pts',(137.676353985377,-5.91679874913726,334.869062031968));
#11709=CARTESIAN_POINT('Ctrl Pts',(137.670052004703,-5.9167495966891,335.002184623396));
#11710=CARTESIAN_POINT('',(135.920052004703,-5.91701510194892,334.994566743858));
#11711=CARTESIAN_POINT('Ctrl Pts',(137.670052004703,-5.92552048316578,335.002187861844));
#11712=CARTESIAN_POINT('Ctrl Pts',(137.664358987021,-5.92609142514278,335.122625259287));
#11713=CARTESIAN_POINT('Ctrl Pts',(137.658665969338,-5.92273849818748,335.243030259708));
#11714=CARTESIAN_POINT('Ctrl Pts',(137.560226940231,-5.79517465950716,337.320703036502));
#11715=CARTESIAN_POINT('Ctrl Pts',(137.374734917381,-3.4185942150446,341.10457504779));
#11716=CARTESIAN_POINT('Ctrl Pts',(137.096496883108,3.28346990442389,341.178304646741));
#11717=CARTESIAN_POINT('Ctrl Pts',(136.818258848833,6.9723421565426,335.58229526301));
#11718=CARTESIAN_POINT('Ctrl Pts',(136.540020814561,4.26279892320134,329.451922111074));
#11719=CARTESIAN_POINT('Ctrl Pts',(136.261782780286,-2.35865196315249,328.412938148315));
#11720=CARTESIAN_POINT('Ctrl Pts',(136.055126510334,-5.66897159192276,332.13095423252));
#11721=CARTESIAN_POINT('Ctrl Pts',(135.941216251806,-5.92117244379854,334.545155774113));
#11722=CARTESIAN_POINT('Ctrl Pts',(135.920052004703,-5.91701510194892,334.994566743858));
#11723=CARTESIAN_POINT('',(134.170052004703,-5.90701886447581,335.000579480333));
#11724=CARTESIAN_POINT('Ctrl Pts',(135.920052004703,-5.91701510194892,334.994566743858));
#11725=CARTESIAN_POINT('Ctrl Pts',(135.848470240382,-5.90295413096146,336.514565540108));
#11726=CARTESIAN_POINT('Ctrl Pts',(135.684142464635,-4.53096395093087,340.026512027423));
#11727=CARTESIAN_POINT('Ctrl Pts',(135.427068677465,1.38457380943765,341.858248922823));
#11728=CARTESIAN_POINT('Ctrl Pts',(135.14883064319,6.51652016864368,337.547074363439));
#11729=CARTESIAN_POINT('Ctrl Pts',(134.870592608916,5.66835215276419,330.898487255479));
#11730=CARTESIAN_POINT('Ctrl Pts',(134.592354574642,-0.381578968966501,
328.013797854939));
#11731=CARTESIAN_POINT('Ctrl Pts',(134.358841039905,-5.16515039241891,330.973395682556));
#11732=CARTESIAN_POINT('Ctrl Pts',(134.218073516592,-5.9061263129331,333.97650851601));
#11733=CARTESIAN_POINT('Ctrl Pts',(134.170052004703,-5.90701886447581,335.000579480333));
#11734=CARTESIAN_POINT('',(132.42005275816,-5.91838694893146,335.005182949526));
#11735=CARTESIAN_POINT('Ctrl Pts',(134.170052004703,-5.90701886447581,335.000579480333));
#11736=CARTESIAN_POINT('Ctrl Pts',(134.125327505167,-5.90785013611822,335.954340817035));
#11737=CARTESIAN_POINT('Ctrl Pts',(133.987856994207,-5.23884552278572,338.884834317021));
#11738=CARTESIAN_POINT('Ctrl Pts',(133.75764047182,-0.629385110448728,341.96824922803));
#11739=CARTESIAN_POINT('Ctrl Pts',(133.479402437547,5.51915303955582,339.300182862063));
#11740=CARTESIAN_POINT('Ctrl Pts',(133.201164403272,6.60284590772511,332.685902154172));
#11741=CARTESIAN_POINT('Ctrl Pts',(132.922926368998,1.62720454421991,328.195234883371));
#11742=CARTESIAN_POINT('Ctrl Pts',(132.662555937229,-4.42628508806817,329.836565795096));
#11743=CARTESIAN_POINT('Ctrl Pts',(132.494931516886,-5.90453803129754,333.416645424348));
#11744=CARTESIAN_POINT('Ctrl Pts',(132.420053107966,-5.91914799116607,335.005176197054));
#11745=CARTESIAN_POINT('',(130.670050602533,-5.92092256589507,334.996739404803));
#11746=CARTESIAN_POINT('Ctrl Pts',(132.420052004703,-5.91674771716332,335.005197493878));
#11747=CARTESIAN_POINT('Ctrl Pts',(132.409195503532,-5.91654548053808,335.23542058194));
#11748=CARTESIAN_POINT('Ctrl Pts',(132.39833900236,-5.90290294749101,335.465076387483));
#11749=CARTESIAN_POINT('Ctrl Pts',(132.387482501188,-5.87603693698799,335.692907264829));
#11750=CARTESIAN_POINT('Ctrl Pts',(132.380471767609,-5.85868784458893,335.840032158642));
#11751=CARTESIAN_POINT('Ctrl Pts',(132.37346103403,-5.8358253124178,335.9863969032));
#11752=CARTESIAN_POINT('Ctrl Pts',(132.366450300451,-5.80751716224808,336.13166910919));
#11753=CARTESIAN_POINT('Ctrl Pts',(132.359026323013,-5.77754040363806,336.285504305964));
#11754=CARTESIAN_POINT('Ctrl Pts',(132.351602345575,-5.74140179668153,336.438379667599));
#11755=CARTESIAN_POINT('Ctrl Pts',(132.344178368137,-5.69917399358948,336.589762986515));
#11756=CARTESIAN_POINT('Ctrl Pts',(132.336763152109,-5.65699602565854,336.740967650338));
#11757=CARTESIAN_POINT('Ctrl Pts',(132.329347936081,-5.6087432650755,336.890683420422));
#11758=CARTESIAN_POINT('Ctrl Pts',(132.321932720054,-5.55453965787506,337.038386555978));
#11759=CARTESIAN_POINT('Ctrl Pts',(132.31452463891,-5.50038820511271,337.185947572321));
#11760=CARTESIAN_POINT('Ctrl Pts',(132.307116557766,-5.44029743259817,337.331499461419));
#11761=CARTESIAN_POINT('Ctrl Pts',(132.299708476621,-5.3744415119523,337.474532076394));
#11762=CARTESIAN_POINT('Ctrl Pts',(132.292305909447,-5.30863460907078,337.617458229582));
#11763=CARTESIAN_POINT('Ctrl Pts',(132.284903342273,-5.23707125769066,337.757868504776));
#11764=CARTESIAN_POINT('Ctrl Pts',(132.277500775099,-5.15997426631245,337.895271340219));
#11765=CARTESIAN_POINT('Ctrl Pts',(132.270102105345,-5.08291786616336,338.032601833669));
#11766=CARTESIAN_POINT('Ctrl Pts',(132.26270343559,-5.00033381046468,338.166927716154));
#11767=CARTESIAN_POINT('Ctrl Pts',(132.255304765835,-4.9124914523721,338.297780813346));
#11768=CARTESIAN_POINT('Ctrl Pts',(132.247907316631,-4.82466358554092,338.42861232384));
#11769=CARTESIAN_POINT('Ctrl Pts',(132.240509867427,-4.73157934574908,338.555971876501));
#11770=CARTESIAN_POINT('Ctrl Pts',(132.233112418223,-4.63355219558828,338.679419059207));
#11771=CARTESIAN_POINT('Ctrl Pts',(132.22571528976,-4.53552929571385,338.802860889459));
#11772=CARTESIAN_POINT('Ctrl Pts',(132.218318161296,-4.43256414368824,338.922390394772));
#11773=CARTESIAN_POINT('Ctrl Pts',(132.210921032833,-4.32501122064948,339.037599349088));
#11774=CARTESIAN_POINT('Ctrl Pts',(132.203522765396,-4.21744173714538,339.152826042707));
#11775=CARTESIAN_POINT('Ctrl Pts',(132.196124497959,-4.10528333078379,339.26373058789));
#11776=CARTESIAN_POINT('Ctrl Pts',(132.188726230523,-3.9889280375635,339.369940923358));
#11777=CARTESIAN_POINT('Ctrl Pts',(132.181325363997,-3.8725318675053,339.476188571634));
#11778=CARTESIAN_POINT('Ctrl Pts',(132.173924497471,-3.75193615050908,339.577738475338));
#11779=CARTESIAN_POINT('Ctrl Pts',(132.166523630946,-3.62756661948799,339.674258335145));
#11780=CARTESIAN_POINT('Ctrl Pts',(132.159114637561,-3.50306051883133,339.770884182987));
#11781=CARTESIAN_POINT('Ctrl Pts',(132.151705644176,-3.3747726233577,339.862468727317));
#11782=CARTESIAN_POINT('Ctrl Pts',(132.144296650791,-3.24315891061265,339.948722142434));
#11783=CARTESIAN_POINT('Ctrl Pts',(132.136883093211,-3.11146411928061,340.035028692629));
#11784=CARTESIAN_POINT('Ctrl Pts',(132.129469535631,-2.97643974746237,340.115997378002));
#11785=CARTESIAN_POINT('Ctrl Pts',(132.122055978051,-2.83856660751528,340.191384225541));
#11786=CARTESIAN_POINT('Ctrl Pts',(132.114631865914,-2.70049717991261,340.266878400059));
#11787=CARTESIAN_POINT('Ctrl Pts',(132.107207753777,-2.55957121749573,340.336774700076));
#11788=CARTESIAN_POINT('Ctrl Pts',(132.09978364164,-2.41629048756569,340.400876858641));
#11789=CARTESIAN_POINT('Ctrl Pts',(132.095926516486,-2.34185037979742,340.434180510807));
#11790=CARTESIAN_POINT('Ctrl Pts',(132.092069391332,-2.2667749461058,340.465921009197));
#11791=CARTESIAN_POINT('Ctrl Pts',(132.088212266178,-2.19113607473682,340.496076169822));
#11792=CARTESIAN_POINT('Ctrl Pts',(132.08078828874,-2.0455506316899,340.554117126017));
#11793=CARTESIAN_POINT('Ctrl Pts',(132.073364311302,-1.8974378047827,340.60645703061));
#11794=CARTESIAN_POINT('Ctrl Pts',(132.065940333864,-1.74728445500175,340.652868970338));
#11795=CARTESIAN_POINT('Ctrl Pts',(132.058525117836,-1.59730830876518,340.699226136994));
#11796=CARTESIAN_POINT('Ctrl Pts',(132.051109901808,-1.44529678616297,340.739669155073));
#11797=CARTESIAN_POINT('Ctrl Pts',(132.043694685781,-1.29175738630769,340.774018827248));
#11798=CARTESIAN_POINT('Ctrl Pts',(132.036286604637,-1.13836572128988,340.808335448343));
#11799=CARTESIAN_POINT('Ctrl Pts',(132.028878523493,-0.983449467519565,
340.836570314711));
#11800=CARTESIAN_POINT('Ctrl Pts',(132.021470442348,-0.827531872647,340.858593821238));
#11801=CARTESIAN_POINT('Ctrl Pts',(132.014067875174,-0.671730330088032,
340.880600935268));
#11802=CARTESIAN_POINT('Ctrl Pts',(132.006665308,-0.514929298420526,340.896405843003));
#11803=CARTESIAN_POINT('Ctrl Pts',(131.999262740826,-0.35766271687783,340.905929896592));
#11804=CARTESIAN_POINT('Ctrl Pts',(131.991864071072,-0.200478935502596,
340.915448935808));
#11805=CARTESIAN_POINT('Ctrl Pts',(131.984465401317,-0.042830463993784,
340.918693684148));
#11806=CARTESIAN_POINT('Ctrl Pts',(131.977066731562,0.11474323742012,340.915637290433));
#11807=CARTESIAN_POINT('Ctrl Pts',(131.969669282358,0.272290944065933,340.912581400929));
#11808=CARTESIAN_POINT('Ctrl Pts',(131.962271833154,0.429763532319038,340.903226439658));
#11809=CARTESIAN_POINT('Ctrl Pts',(131.95487438395,0.586621017634842,340.887597671731));
#11810=CARTESIAN_POINT('Ctrl Pts',(131.947477255487,0.743471701883489,340.87196958144));
#11811=CARTESIAN_POINT('Ctrl Pts',(131.940080127023,0.899706964850715,340.850068262363));
#11812=CARTESIAN_POINT('Ctrl Pts',(131.93268299856,1.05479169045151,340.821970890708));
#11813=CARTESIAN_POINT('Ctrl Pts',(131.925284731123,1.20990029522872,340.79386919276));
#11814=CARTESIAN_POINT('Ctrl Pts',(131.917886463687,1.36385764264725,340.759569609156));
#11815=CARTESIAN_POINT('Ctrl Pts',(131.91048819625,1.51613870526667,340.719200467626));
#11816=CARTESIAN_POINT('Ctrl Pts',(131.903087329724,1.66847326582496,340.678817143992));
#11817=CARTESIAN_POINT('Ctrl Pts',(131.895686463198,1.81913000856909,340.6323601126));
#11818=CARTESIAN_POINT('Ctrl Pts',(131.888285596673,1.96759910739992,340.580007555108));
#11819=CARTESIAN_POINT('Ctrl Pts',(131.880876603288,2.11623123949537,340.527597509502));
#11820=CARTESIAN_POINT('Ctrl Pts',(131.873467609903,2.26267057809113,340.469279133354));
#11821=CARTESIAN_POINT('Ctrl Pts',(131.866058616518,2.40642664695764,340.405279026592));
#11822=CARTESIAN_POINT('Ctrl Pts',(131.858645058938,2.5502712745213,340.341239493556));
#11823=CARTESIAN_POINT('Ctrl Pts',(131.851231501358,2.69142900472983,340.271511420314));
#11824=CARTESIAN_POINT('Ctrl Pts',(131.843817943777,2.82943448031721,340.196367104439));
#11825=CARTESIAN_POINT('Ctrl Pts',(131.836393831641,2.96763643196422,340.121115806873));
#11826=CARTESIAN_POINT('Ctrl Pts',(131.828969719504,3.10267684641389,340.040433057142));
#11827=CARTESIAN_POINT('Ctrl Pts',(131.821545607367,3.23411914352195,339.954634590765));
#11828=CARTESIAN_POINT('Ctrl Pts',(131.817688482213,3.30240870882434,339.910058833179));
#11829=CARTESIAN_POINT('Ctrl Pts',(131.813831357058,3.3697275960796,339.864102904267));
#11830=CARTESIAN_POINT('Ctrl Pts',(131.809974231903,3.43601824744375,339.81681525136));
#11831=CARTESIAN_POINT('Ctrl Pts',(131.802550254465,3.56361076268136,339.725798638159));
#11832=CARTESIAN_POINT('Ctrl Pts',(131.795126277027,3.68777685442863,339.629571527803));
#11833=CARTESIAN_POINT('Ctrl Pts',(131.787702299589,3.80806223806477,339.528420536294));
#11834=CARTESIAN_POINT('Ctrl Pts',(131.780287083562,3.92820566685031,339.427388918174));
#11835=CARTESIAN_POINT('Ctrl Pts',(131.772871867534,4.04447722086647,339.321445223496));
#11836=CARTESIAN_POINT('Ctrl Pts',(131.765456651506,4.15645157236773,339.210919245137));
#11837=CARTESIAN_POINT('Ctrl Pts',(131.758048570362,4.26831818271177,339.100499614317));
#11838=CARTESIAN_POINT('Ctrl Pts',(131.750640489218,4.37589555821339,338.985506737836));
#11839=CARTESIAN_POINT('Ctrl Pts',(131.743232408074,4.47879155183845,338.866310489043));
#11840=CARTESIAN_POINT('Ctrl Pts',(131.7358298409,4.58161095809617,338.747202960194));
#11841=CARTESIAN_POINT('Ctrl Pts',(131.728427273726,4.67975567766997,338.623898569922));
#11842=CARTESIAN_POINT('Ctrl Pts',(131.721024706552,4.77287062874716,338.496803758254));
#11843=CARTESIAN_POINT('Ctrl Pts',(131.713626036797,4.86593655520969,338.36977586145));
#11844=CARTESIAN_POINT('Ctrl Pts',(131.706227367043,4.95397776711305,338.238961817986));
#11845=CARTESIAN_POINT('Ctrl Pts',(131.698828697288,5.03667975184522,338.104800740765));
#11846=CARTESIAN_POINT('Ctrl Pts',(131.691431248084,5.11936809331791,337.970661795955));
#11847=CARTESIAN_POINT('Ctrl Pts',(131.68403379888,5.1967187600848,337.833177230632));
#11848=CARTESIAN_POINT('Ctrl Pts',(131.676636349676,5.26846078149481,337.692814801718));
#11849=CARTESIAN_POINT('Ctrl Pts',(131.669239221213,5.34019969229583,337.552458458674));
#11850=CARTESIAN_POINT('Ctrl Pts',(131.661842092749,5.40633027140921,337.409224832462));
#11851=CARTESIAN_POINT('Ctrl Pts',(131.654444964286,5.46662783593587,337.263605678088));
#11852=CARTESIAN_POINT('Ctrl Pts',(131.647046696849,5.52693468478226,337.117964101998));
#11853=CARTESIAN_POINT('Ctrl Pts',(131.639648429412,5.58140658793936,336.969936611221));
#11854=CARTESIAN_POINT('Ctrl Pts',(131.632250161976,5.62986733645778,336.820034158027));
#11855=CARTESIAN_POINT('Ctrl Pts',(131.62484929545,5.67834510974678,336.670079042526));
#11856=CARTESIAN_POINT('Ctrl Pts',(131.617448428924,5.72080740911297,336.518248008041));
#11857=CARTESIAN_POINT('Ctrl Pts',(131.610047562399,5.75712817515735,336.365066202537));
#11858=CARTESIAN_POINT('Ctrl Pts',(131.602638569014,5.79348882487528,336.211716188766));
#11859=CARTESIAN_POINT('Ctrl Pts',(131.595229575629,5.82369438700597,336.057012805153));
#11860=CARTESIAN_POINT('Ctrl Pts',(131.587820582244,5.84766998943229,335.901491129847));
#11861=CARTESIAN_POINT('Ctrl Pts',(131.580407024664,5.87166036165672,335.745873647825));
#11862=CARTESIAN_POINT('Ctrl Pts',(131.572993467084,5.88941308472895,335.589437239597));
#11863=CARTESIAN_POINT('Ctrl Pts',(131.565579909504,5.90090530796868,335.432720589858));
#11864=CARTESIAN_POINT('Ctrl Pts',(131.558155797367,5.91241389249212,335.275780825277));
#11865=CARTESIAN_POINT('Ctrl Pts',(131.55073168523,5.91764416382847,335.118560394351));
#11866=CARTESIAN_POINT('Ctrl Pts',(131.543307573094,5.91662537214471,334.961597289243));
#11867=CARTESIAN_POINT('Ctrl Pts',(131.539450447939,5.91609606884776,334.880048636699));
#11868=CARTESIAN_POINT('Ctrl Pts',(131.535593322784,5.91388086044975,334.798569358136));
#11869=CARTESIAN_POINT('Ctrl Pts',(131.531736197629,5.90998933949256,334.717234072802));
#11870=CARTESIAN_POINT('Ctrl Pts',(131.524312220191,5.90249915894961,334.560684492736));
#11871=CARTESIAN_POINT('Ctrl Pts',(131.516888242753,5.88877312582884,334.404196566294));
#11872=CARTESIAN_POINT('Ctrl Pts',(131.509464265315,5.86880642216648,334.24830741547));
#11873=CARTESIAN_POINT('Ctrl Pts',(131.502049049288,5.8488632822186,334.092602237299));
#11874=CARTESIAN_POINT('Ctrl Pts',(131.49463383326,5.82269417869338,333.937494794744));
#11875=CARTESIAN_POINT('Ctrl Pts',(131.487218617233,5.79034627220662,333.783521224828));
#11876=CARTESIAN_POINT('Ctrl Pts',(131.479810536088,5.7580294907126,333.629695807507));
#11877=CARTESIAN_POINT('Ctrl Pts',(131.472402454944,5.71954581828712,333.477002453631));
#11878=CARTESIAN_POINT('Ctrl Pts',(131.4649943738,5.67499407605729,333.325971087701));
#11879=CARTESIAN_POINT('Ctrl Pts',(131.457591806626,5.63047549450289,333.175052137174));
#11880=CARTESIAN_POINT('Ctrl Pts',(131.450189239452,5.57989794144367,333.025793067878));
#11881=CARTESIAN_POINT('Ctrl Pts',(131.442786672278,5.5234110458261,332.878712423704));
#11882=CARTESIAN_POINT('Ctrl Pts',(131.435388002523,5.46695389031218,332.731709216847));
#11883=CARTESIAN_POINT('Ctrl Pts',(131.427989332769,5.40459372193263,332.586882498454));
#11884=CARTESIAN_POINT('Ctrl Pts',(131.420590663014,5.33652959927374,332.444734378078));
#11885=CARTESIAN_POINT('Ctrl Pts',(131.41319321381,5.26847670508156,332.302609707728));
#11886=CARTESIAN_POINT('Ctrl Pts',(131.405795764606,5.19472188516404,332.16316309468));
#11887=CARTESIAN_POINT('Ctrl Pts',(131.398398315402,5.1155118485306,332.026875534048));
#11888=CARTESIAN_POINT('Ctrl Pts',(131.391001186939,5.03630524630629,331.890593882607));
#11889=CARTESIAN_POINT('Ctrl Pts',(131.383604058475,4.95164408519902,331.757471333909));
#11890=CARTESIAN_POINT('Ctrl Pts',(131.376206930012,4.86182030367583,331.627962945449));
#11891=CARTESIAN_POINT('Ctrl Pts',(131.368808662575,4.77198269153254,331.49843461593));
#11892=CARTESIAN_POINT('Ctrl Pts',(131.361410395138,4.67698108890476,331.372521861382));
#11893=CARTESIAN_POINT('Ctrl Pts',(131.354012127702,4.57714980968615,331.250649365265));
#11894=CARTESIAN_POINT('Ctrl Pts',(131.346611261176,4.4772834586893,331.128734054057));
#11895=CARTESIAN_POINT('Ctrl Pts',(131.33921039465,4.3725842892917,331.010862115805));
#11896=CARTESIAN_POINT('Ctrl Pts',(131.331809528124,4.26342569164432,330.89742374424));
#11897=CARTESIAN_POINT('Ctrl Pts',(131.32440053474,4.15414722742063,330.783860806498));
#11898=CARTESIAN_POINT('Ctrl Pts',(131.316991541355,4.04039981455201,330.674741427143));
#11899=CARTESIAN_POINT('Ctrl Pts',(131.30958254797,3.92259289407055,330.570418129226));
#11900=CARTESIAN_POINT('Ctrl Pts',(131.30216899039,3.80471340046252,330.466030564559));
#11901=CARTESIAN_POINT('Ctrl Pts',(131.29475543281,3.68276970446464,330.366445204179));
#11902=CARTESIAN_POINT('Ctrl Pts',(131.287341875229,3.55720243171438,330.271972776907));
#11903=CARTESIAN_POINT('Ctrl Pts',(131.279917763093,3.43145639096328,330.17736585084));
#11904=CARTESIAN_POINT('Ctrl Pts',(131.272493650956,3.30207677637937,330.08788660761));
#11905=CARTESIAN_POINT('Ctrl Pts',(131.265069538819,3.1695318259944,330.003801588557));
#11906=CARTESIAN_POINT('Ctrl Pts',(131.261212413665,3.10066938792222,329.96011603584));
#11907=CARTESIAN_POINT('Ctrl Pts',(131.25735528851,3.03095294792238,329.917885738931));
#11908=CARTESIAN_POINT('Ctrl Pts',(131.253498163355,2.96045044598856,329.877143012015));
#11909=CARTESIAN_POINT('Ctrl Pts',(131.246074185917,2.82475119779435,329.798723704043));
#11910=CARTESIAN_POINT('Ctrl Pts',(131.238650208479,2.6857292178045,329.725581621853));
#11911=CARTESIAN_POINT('Ctrl Pts',(131.231226231041,2.54383357608647,329.658011484505));
#11912=CARTESIAN_POINT('Ctrl Pts',(131.223811015014,2.40210539257502,329.590521090086));
#11913=CARTESIAN_POINT('Ctrl Pts',(131.216395798986,2.25751063155815,329.528589710304));
#11914=CARTESIAN_POINT('Ctrl Pts',(131.208980582958,2.11052566341192,329.472467821299));
#11915=CARTESIAN_POINT('Ctrl Pts',(131.201572501814,1.96368212346207,329.416399932492));
#11916=CARTESIAN_POINT('Ctrl Pts',(131.19416442067,1.81445330127638,329.366130538323));
#11917=CARTESIAN_POINT('Ctrl Pts',(131.186756339526,1.66333829945345,329.321863310551));
#11918=CARTESIAN_POINT('Ctrl Pts',(131.179353772352,1.51233577528602,329.277629031684));
#11919=CARTESIAN_POINT('Ctrl Pts',(131.171951205178,1.35945022351259,329.239388128197));
#11920=CARTESIAN_POINT('Ctrl Pts',(131.164548638004,1.20519867156313,329.207295387769));
#11921=CARTESIAN_POINT('Ctrl Pts',(131.157149968249,1.05102833238162,329.175219544029));
#11922=CARTESIAN_POINT('Ctrl Pts',(131.149751298495,0.89549378980647,329.149285492537));
#11923=CARTESIAN_POINT('Ctrl Pts',(131.14235262874,0.739125000495771,329.129597560972));
#11924=CARTESIAN_POINT('Ctrl Pts',(131.134955179536,0.582782007179798,329.109912877305));
#11925=CARTESIAN_POINT('Ctrl Pts',(131.127557730332,0.425605410196819,329.096472315099));
#11926=CARTESIAN_POINT('Ctrl Pts',(131.120160281128,0.268133197000217,329.089328705539));
#11927=CARTESIAN_POINT('Ctrl Pts',(131.112763152664,0.110667811524301,329.082185405714));
#11928=CARTESIAN_POINT('Ctrl Pts',(131.105366024201,-0.0470927918521481,
329.081338532585));
#11929=CARTESIAN_POINT('Ctrl Pts',(131.097968895738,-0.204607960918182,
329.086788846589));
#11930=CARTESIAN_POINT('Ctrl Pts',(131.090570628301,-0.362147383388201,
329.092239999805));
#11931=CARTESIAN_POINT('Ctrl Pts',(131.083172360864,-0.519440923290675,
329.103990257867));
#11932=CARTESIAN_POINT('Ctrl Pts',(131.075774093428,-0.675950538814617,
329.121988309677));
#11933=CARTESIAN_POINT('Ctrl Pts',(131.068373226902,-0.832515137812552,
329.139992684392));
#11934=CARTESIAN_POINT('Ctrl Pts',(131.060972360376,-0.988294893575073,
329.164249180318));
#11935=CARTESIAN_POINT('Ctrl Pts',(131.05357149385,-1.14275962103158,329.19465496193));
#11936=CARTESIAN_POINT('Ctrl Pts',(131.046162500466,-1.29739396552618,329.225094131998));
#11937=CARTESIAN_POINT('Ctrl Pts',(131.038753507081,-1.45071003151352,329.261696000736));
#11938=CARTESIAN_POINT('Ctrl Pts',(131.031344513696,-1.6021898028041,329.304307030897));
#11939=CARTESIAN_POINT('Ctrl Pts',(131.023930956116,-1.75376289085883,329.346944310922));
#11940=CARTESIAN_POINT('Ctrl Pts',(131.016517398536,-1.90349707599541,329.395598013733));
#11941=CARTESIAN_POINT('Ctrl Pts',(131.009103840955,-2.0508926119025,329.450065761025));
#11942=CARTESIAN_POINT('Ctrl Pts',(131.001679728819,-2.19849799233933,329.504611053128));
#11943=CARTESIAN_POINT('Ctrl Pts',(130.994255616682,-2.34375773017976,329.564986778395));
#11944=CARTESIAN_POINT('Ctrl Pts',(130.986831504545,-2.48619429465784,329.630943426289));
#11945=CARTESIAN_POINT('Ctrl Pts',(130.982974379391,-2.56019582449433,329.665210560328));
#11946=CARTESIAN_POINT('Ctrl Pts',(130.979117254236,-2.63343574812116,329.700983365228));
#11947=CARTESIAN_POINT('Ctrl Pts',(130.975260129081,-2.70585012562227,329.738222195857));
#11948=CARTESIAN_POINT('Ctrl Pts',(130.967836151643,-2.84522924431737,329.809897401438));
#11949=CARTESIAN_POINT('Ctrl Pts',(130.960412174205,-2.98196875210054,329.88722257275));
#11950=CARTESIAN_POINT('Ctrl Pts',(130.952988196767,-3.1155777958457,329.969979566589));
#11951=CARTESIAN_POINT('Ctrl Pts',(130.94557298074,-3.24902916081658,330.052638894723));
#11952=CARTESIAN_POINT('Ctrl Pts',(130.938157764712,-3.37935710135488,330.140717090834));
#11953=CARTESIAN_POINT('Ctrl Pts',(130.930742548685,-3.50609319538716,330.233949111921));
#11954=CARTESIAN_POINT('Ctrl Pts',(130.92333446754,-3.63270734458783,330.327091425626));
#11955=CARTESIAN_POINT('Ctrl Pts',(130.915926386396,-3.75573622902762,330.425377472217));
#11956=CARTESIAN_POINT('Ctrl Pts',(130.908518305252,-3.87473848372444,330.528497764146));
#11957=CARTESIAN_POINT('Ctrl Pts',(130.901115738078,-3.99365216286977,330.631541301759));
#11958=CARTESIAN_POINT('Ctrl Pts',(130.893713170904,-4.10854489908171,330.739411676776));
#11959=CARTESIAN_POINT('Ctrl Pts',(130.88631060373,-4.21900673488797,330.851757874295));
#11960=CARTESIAN_POINT('Ctrl Pts',(130.878911933976,-4.32941041302072,330.964044922034));
#11961=CARTESIAN_POINT('Ctrl Pts',(130.871513264221,-4.43538757575636,331.080802833711));
#11962=CARTESIAN_POINT('Ctrl Pts',(130.864114594466,-4.53656370176803,331.201642415161));
#11963=CARTESIAN_POINT('Ctrl Pts',(130.856717145262,-4.63772313686048,331.322462061833));
#11964=CARTESIAN_POINT('Ctrl Pts',(130.849319696058,-4.73408286778036,331.447361756022));
#11965=CARTESIAN_POINT('Ctrl Pts',(130.841922246854,-4.82530733177565,331.575917682588));
#11966=CARTESIAN_POINT('Ctrl Pts',(130.834525118391,-4.91652784043711,331.704468035193));
#11967=CARTESIAN_POINT('Ctrl Pts',(130.827127989927,-5.0026133089068,331.836674000604));
#11968=CARTESIAN_POINT('Ctrl Pts',(130.819730861464,-5.08327051978381,331.972081344356));
#11969=CARTESIAN_POINT('Ctrl Pts',(130.812332594027,-5.16394014985785,332.107509537459));
#11970=CARTESIAN_POINT('Ctrl Pts',(130.804934326591,-5.23917966711533,332.24613976974));
#11971=CARTESIAN_POINT('Ctrl Pts',(130.797536059154,-5.30874105485643,332.387491822983));
#11972=CARTESIAN_POINT('Ctrl Pts',(130.790135192628,-5.37832688024466,332.528893534688));
#11973=CARTESIAN_POINT('Ctrl Pts',(130.782734326102,-5.4422304398142,332.673018636507));
#11974=CARTESIAN_POINT('Ctrl Pts',(130.775333459577,-5.50025129658857,332.819365634299));
#11975=CARTESIAN_POINT('Ctrl Pts',(130.767924466192,-5.5583358658107,332.965873335086));
#11976=CARTESIAN_POINT('Ctrl Pts',(130.760515472807,-5.61052469410175,333.114607457219));
#11977=CARTESIAN_POINT('Ctrl Pts',(130.753106479422,-5.656666565926,333.265049302016));
#11978=CARTESIAN_POINT('Ctrl Pts',(130.745692921842,-5.70283686273494,333.415583824179));
#11979=CARTESIAN_POINT('Ctrl Pts',(130.738279364262,-5.74295268538358,333.567827805239));
#11980=CARTESIAN_POINT('Ctrl Pts',(130.730865806682,-5.77691377670035,333.721251479348));
#11981=CARTESIAN_POINT('Ctrl Pts',(130.723441694545,-5.81092321784797,333.874893580145));
#11982=CARTESIAN_POINT('Ctrl Pts',(130.716017582408,-5.83876036155908,334.029718361975));
#11983=CARTESIAN_POINT('Ctrl Pts',(130.708593470272,-5.86037660726913,334.185189234563));
#11984=CARTESIAN_POINT('Ctrl Pts',(130.704736345117,-5.87160711720014,334.265962612234));
#11985=CARTESIAN_POINT('Ctrl Pts',(130.700879219962,-5.88115932756141,334.346910343893));
#11986=CARTESIAN_POINT('Ctrl Pts',(130.697022094807,-5.88903197523169,334.427957206847));
#11987=CARTESIAN_POINT('Ctrl Pts',(130.688032064773,-5.90738122141063,334.616857930293));
#11988=CARTESIAN_POINT('Ctrl Pts',(130.679042034738,-5.91664347140671,334.806655501886));
#11989=CARTESIAN_POINT('Ctrl Pts',(130.670052004703,-5.91674908643611,334.996712043568));
#11990=CARTESIAN_POINT('',(128.920053149077,-5.91243296764551,334.996538828883));
#11991=CARTESIAN_POINT('Ctrl Pts',(130.670049495371,-5.92421797011413,334.996761009397));
#11992=CARTESIAN_POINT('Ctrl Pts',(130.586294350425,-5.9123736713581,336.769655413876));
#11993=CARTESIAN_POINT('Ctrl Pts',(130.409793194054,-4.12388091182169,340.526437395856));
#11994=CARTESIAN_POINT('Ctrl Pts',(130.14054602626,2.26943811269259,341.618328608785));
#11995=CARTESIAN_POINT('Ctrl Pts',(129.862307991985,6.79361690608675,336.673138444528));
#11996=CARTESIAN_POINT('Ctrl Pts',(129.584069957711,5.08339373838535,330.192533825209));
#11997=CARTESIAN_POINT('Ctrl Pts',(129.305831923437,-1.29178483226323,328.123669956412));
#11998=CARTESIAN_POINT('Ctrl Pts',(129.084493291078,-5.42021756930977,331.497741847142));
#11999=CARTESIAN_POINT('Ctrl Pts',(128.955900670143,-5.91301563696258,334.232721977575));
#12000=CARTESIAN_POINT('Ctrl Pts',(128.920054060632,-5.90899501774148,334.996521404454));
#12001=CARTESIAN_POINT('',(127.170050856975,-5.91375951636249,335.004785277391));
#12002=CARTESIAN_POINT('Ctrl Pts',(128.920052004703,-5.91674900040053,334.996560703666));
#12003=CARTESIAN_POINT('Ctrl Pts',(128.912579712844,-5.91684167049648,335.155984505595));
#12004=CARTESIAN_POINT('Ctrl Pts',(128.905107420984,-5.91048660953891,335.315420720306));
#12005=CARTESIAN_POINT('Ctrl Pts',(128.897635129125,-5.89770744149063,335.474317928278));
#12006=CARTESIAN_POINT('Ctrl Pts',(128.890161693573,-5.88492631749113,335.633239456705));
#12007=CARTESIAN_POINT('Ctrl Pts',(128.882688258021,-5.8657191558017,335.791621452473));
#12008=CARTESIAN_POINT('Ctrl Pts',(128.875214822469,-5.84016151511452,335.948917298754));
#12009=CARTESIAN_POINT('Ctrl Pts',(128.867738883119,-5.81459531194363,336.106265843293));
#12010=CARTESIAN_POINT('Ctrl Pts',(128.860262943769,-5.78267444888914,336.262527155498));
#12011=CARTESIAN_POINT('Ctrl Pts',(128.852787004419,-5.74452568383359,336.417164503604));
#12012=CARTESIAN_POINT('Ctrl Pts',(128.845307199907,-5.70635719535002,336.571881801314));
#12013=CARTESIAN_POINT('Ctrl Pts',(128.837827395396,-5.6619544764055,336.724973110494));
#12014=CARTESIAN_POINT('Ctrl Pts',(128.830347590884,-5.61149423945202,336.875916566134));
#12015=CARTESIAN_POINT('Ctrl Pts',(128.822857867366,-5.56096708692768,337.027060188641));
#12016=CARTESIAN_POINT('Ctrl Pts',(128.815368143848,-5.50436648500666,337.176049923871));
#12017=CARTESIAN_POINT('Ctrl Pts',(128.80787842033,-5.44191779758709,337.322382665885));
#12018=CARTESIAN_POINT('Ctrl Pts',(128.800383220738,-5.37942345111426,337.46882239837));
#12019=CARTESIAN_POINT('Ctrl Pts',(128.792888021145,-5.31107265074541,337.612600938451));
#12020=CARTESIAN_POINT('Ctrl Pts',(128.785392821553,-5.23713674329087,337.753239781525));
#12021=CARTESIAN_POINT('Ctrl Pts',(128.777885565949,-5.16308191010289,337.894104841848));
#12022=CARTESIAN_POINT('Ctrl Pts',(128.770378310346,-5.08342420267718,338.031819802281));
#12023=CARTESIAN_POINT('Ctrl Pts',(128.762871054742,-4.9984788934223,338.165934193017));
#12024=CARTESIAN_POINT('Ctrl Pts',(128.758365988124,-4.94750363731544,338.246415569509));
#12025=CARTESIAN_POINT('Ctrl Pts',(128.753860921507,-4.8946250466006,338.32560093499));
#12026=CARTESIAN_POINT('Ctrl Pts',(128.749355854889,-4.83991808089027,338.403398820704));
#12027=CARTESIAN_POINT('Ctrl Pts',(128.741931877451,-4.74976552298043,338.531603306294));
#12028=CARTESIAN_POINT('Ctrl Pts',(128.734507900013,-4.65437943888897,338.656416647204));
#12029=CARTESIAN_POINT('Ctrl Pts',(128.727083922575,-4.55404336906196,338.777382632883));
#12030=CARTESIAN_POINT('Ctrl Pts',(128.719668706548,-4.45382571089371,338.898205860498));
#12031=CARTESIAN_POINT('Ctrl Pts',(128.71225349052,-4.34866993099153,339.015190486275));
#12032=CARTESIAN_POINT('Ctrl Pts',(128.704838274492,-4.23890294131249,339.127908964189));
#12033=CARTESIAN_POINT('Ctrl Pts',(128.697430193348,-4.129241568878,339.240518984951));
#12034=CARTESIAN_POINT('Ctrl Pts',(128.690022112204,-4.01497807830944,339.348870764282));
#12035=CARTESIAN_POINT('Ctrl Pts',(128.68261403106,-3.89647968528122,339.452569665338));
#12036=CARTESIAN_POINT('Ctrl Pts',(128.675211463886,-3.77806949277126,339.556191381409));
#12037=CARTESIAN_POINT('Ctrl Pts',(128.667808896712,-3.65543095377422,339.655166870259));
#12038=CARTESIAN_POINT('Ctrl Pts',(128.660406329538,-3.52896810021188,339.749138312388));
#12039=CARTESIAN_POINT('Ctrl Pts',(128.653007659783,-3.40257182878891,339.843060278963));
#12040=CARTESIAN_POINT('Ctrl Pts',(128.645608990029,-3.27235555158258,339.93198322376));
#12041=CARTESIAN_POINT('Ctrl Pts',(128.638210320274,-3.13875624671768,340.015589674823));
#12042=CARTESIAN_POINT('Ctrl Pts',(128.63081287107,-3.00517898158994,340.099182333418));
#12043=CARTESIAN_POINT('Ctrl Pts',(128.623415421866,-2.86822011250208,340.177460041162));
#12044=CARTESIAN_POINT('Ctrl Pts',(128.616017972662,-2.72834555510473,340.250148673556));
#12045=CARTESIAN_POINT('Ctrl Pts',(128.608620844199,-2.58847706242438,340.322834154298));
#12046=CARTESIAN_POINT('Ctrl Pts',(128.601223715735,-2.44569346396151,340.389930869431));
#12047=CARTESIAN_POINT('Ctrl Pts',(128.593826587272,-2.30048498560767,340.451210819029));
#12048=CARTESIAN_POINT('Ctrl Pts',(128.586428319835,-2.15525414877301,340.512500204209));
#12049=CARTESIAN_POINT('Ctrl Pts',(128.579030052399,-2.00759803248398,340.567970895406));
#12050=CARTESIAN_POINT('Ctrl Pts',(128.571631784962,-1.85802638693673,340.617443235846));
#12051=CARTESIAN_POINT('Ctrl Pts',(128.564230918436,-1.70840219529709,340.666932956439));
#12052=CARTESIAN_POINT('Ctrl Pts',(128.556830051911,-1.55686148867438,340.710420013551));
#12053=CARTESIAN_POINT('Ctrl Pts',(128.549429185385,-1.403928551426,340.747774802912));
#12054=CARTESIAN_POINT('Ctrl Pts',(128.542020192,-1.25082767919194,340.785170611403));
#12055=CARTESIAN_POINT('Ctrl Pts',(128.534611198615,-1.09633188600138,340.816420615743));
#12056=CARTESIAN_POINT('Ctrl Pts',(128.527202205231,-0.940975731978278,
340.84144633069));
#12057=CARTESIAN_POINT('Ctrl Pts',(128.51978864765,-0.78552387320538,340.86648746234));
#12058=CARTESIAN_POINT('Ctrl Pts',(128.51237509007,-0.629210967153669,340.885296619612));
#12059=CARTESIAN_POINT('Ctrl Pts',(128.50496153249,-0.47257553185195,340.897847313147));
#12060=CARTESIAN_POINT('Ctrl Pts',(128.497537420353,-0.315717097332351,
340.910415874892));
#12061=CARTESIAN_POINT('Ctrl Pts',(128.490113308217,-0.158535588396375,
340.916708162823));
#12062=CARTESIAN_POINT('Ctrl Pts',(128.48268919608,-0.00156918253640919,
340.916749791918));
#12063=CARTESIAN_POINT('Ctrl Pts',(128.478832070925,0.0799811848830685,
340.91677141991));
#12064=CARTESIAN_POINT('Ctrl Pts',(128.47497494577,0.161473569395059,340.915106712601));
#12065=CARTESIAN_POINT('Ctrl Pts',(128.471117820615,0.242833288648434,340.911764758211));
#12066=CARTESIAN_POINT('Ctrl Pts',(128.463693843177,0.399429897742017,340.905332352469));
#12067=CARTESIAN_POINT('Ctrl Pts',(128.456269865739,0.556006982243015,340.892663819937));
#12068=CARTESIAN_POINT('Ctrl Pts',(128.448845888301,0.712027464962904,340.873750714121));
#12069=CARTESIAN_POINT('Ctrl Pts',(128.441430672274,0.867863820038581,340.854859928616));
#12070=CARTESIAN_POINT('Ctrl Pts',(128.434015456246,1.02314451395496,340.82973928348));
#12071=CARTESIAN_POINT('Ctrl Pts',(128.426600240219,1.17733310332001,340.798432316267));
#12072=CARTESIAN_POINT('Ctrl Pts',(128.419192159074,1.33137333320056,340.76715547246));
#12073=CARTESIAN_POINT('Ctrl Pts',(128.41178407793,1.48432318720783,340.729704230556));
#12074=CARTESIAN_POINT('Ctrl Pts',(128.404375996786,1.63565208532899,340.686173829409));
#12075=CARTESIAN_POINT('Ctrl Pts',(128.396973429612,1.78686834658715,340.642675828736));
#12076=CARTESIAN_POINT('Ctrl Pts',(128.389570862438,1.93646569715959,340.593107781144));
#12077=CARTESIAN_POINT('Ctrl Pts',(128.382168295264,2.08392459413759,340.537615809033));
#12078=CARTESIAN_POINT('Ctrl Pts',(128.37476962551,2.23130585465174,340.482153053202));
#12079=CARTESIAN_POINT('Ctrl Pts',(128.367370955755,2.37655055542424,340.420772715484));
#12080=CARTESIAN_POINT('Ctrl Pts',(128.359972286,2.51915525357791,340.353670457814));
#12081=CARTESIAN_POINT('Ctrl Pts',(128.352574836796,2.66173642638404,340.286579269933));
#12082=CARTESIAN_POINT('Ctrl Pts',(128.345177387592,2.80167812356927,340.213768194262));
#12083=CARTESIAN_POINT('Ctrl Pts',(128.337779938388,2.93849769430178,340.135480684715));
#12084=CARTESIAN_POINT('Ctrl Pts',(128.330382809925,3.07531133277629,340.057196569578));
#12085=CARTESIAN_POINT('Ctrl Pts',(128.322985681461,3.20900279002705,339.973436678043));
#12086=CARTESIAN_POINT('Ctrl Pts',(128.315588552998,3.33911504669222,339.884489867678));
#12087=CARTESIAN_POINT('Ctrl Pts',(128.308190285561,3.46924733739688,339.795529361725));
#12088=CARTESIAN_POINT('Ctrl Pts',(128.300792018125,3.59579902207019,339.701380557347));
#12089=CARTESIAN_POINT('Ctrl Pts',(128.293393750688,3.71834316841695,339.602374891769));
#12090=CARTESIAN_POINT('Ctrl Pts',(128.285992884162,3.84093036581098,339.50333444446));
#12091=CARTESIAN_POINT('Ctrl Pts',(128.278592017636,3.9595069316497,339.399433973172));
#12092=CARTESIAN_POINT('Ctrl Pts',(128.271191151111,4.0736801585877,339.2910442235));
#12093=CARTESIAN_POINT('Ctrl Pts',(128.263782157726,4.18797875864438,339.182535451519));
#12094=CARTESIAN_POINT('Ctrl Pts',(128.256373164341,4.29786409264582,339.069527813475));
#12095=CARTESIAN_POINT('Ctrl Pts',(128.248964170956,4.40298087952114,338.952428359512));
#12096=CARTESIAN_POINT('Ctrl Pts',(128.241550613376,4.50816242196326,338.835256768245));
#12097=CARTESIAN_POINT('Ctrl Pts',(128.234137055796,4.60856932628622,338.713988625025));
#12098=CARTESIAN_POINT('Ctrl Pts',(128.226723498216,4.70388789401863,338.589062446239));
#12099=CARTESIAN_POINT('Ctrl Pts',(128.219299386079,4.7993421651824,338.463958412168));
#12100=CARTESIAN_POINT('Ctrl Pts',(128.211875273942,4.88969341790184,338.335186246033));
#12101=CARTESIAN_POINT('Ctrl Pts',(128.204451161806,4.97467195363788,338.203212374506));
#12102=CARTESIAN_POINT('Ctrl Pts',(128.200594036651,5.01882172424593,338.134646634891));
#12103=CARTESIAN_POINT('Ctrl Pts',(128.196736911496,5.06152204164618,338.065217081547));
#12104=CARTESIAN_POINT('Ctrl Pts',(128.192879786341,5.10274013340856,337.994991434612));
#12105=CARTESIAN_POINT('Ctrl Pts',(128.185455808903,5.18207439688276,337.859825061345));
#12106=CARTESIAN_POINT('Ctrl Pts',(128.178031831465,5.25615400242056,337.721300380689));
#12107=CARTESIAN_POINT('Ctrl Pts',(128.170607854027,5.32468120389963,337.579864461428));
#12108=CARTESIAN_POINT('Ctrl Pts',(128.163192638,5.39312753297071,337.438595457831));
#12109=CARTESIAN_POINT('Ctrl Pts',(128.155777421972,5.45603434003352,337.294422387042));
#12110=CARTESIAN_POINT('Ctrl Pts',(128.148362205944,5.51314793644405,337.147819916423));
#12111=CARTESIAN_POINT('Ctrl Pts',(128.1409541248,5.5702065784394,337.001358505963));
#12112=CARTESIAN_POINT('Ctrl Pts',(128.133546043656,5.62148297239911,336.85247269474));
#12113=CARTESIAN_POINT('Ctrl Pts',(128.126137962512,5.66677007941836,336.701660198015));
#12114=CARTESIAN_POINT('Ctrl Pts',(128.118735395338,5.71202347841697,336.550959953785));
#12115=CARTESIAN_POINT('Ctrl Pts',(128.111332828164,5.7512963599982,336.398336235402));
#12116=CARTESIAN_POINT('Ctrl Pts',(128.10393026099,5.78443044712525,336.244305012796));
#12117=CARTESIAN_POINT('Ctrl Pts',(128.096531591235,5.81754708929998,336.090354886958));
#12118=CARTESIAN_POINT('Ctrl Pts',(128.089132921481,5.84453129554744,335.934999096677));
#12119=CARTESIAN_POINT('Ctrl Pts',(128.081734251726,5.86527516033568,335.778766881711));
#12120=CARTESIAN_POINT('Ctrl Pts',(128.074336802522,5.88601560303051,335.622560440208));
#12121=CARTESIAN_POINT('Ctrl Pts',(128.066939353318,5.90051769834206,335.465478230574));
#12122=CARTESIAN_POINT('Ctrl Pts',(128.059541904114,5.90872498180179,335.308057871075));
#12123=CARTESIAN_POINT('Ctrl Pts',(128.05214477565,5.916931909408,335.150644337049));
#12124=CARTESIAN_POINT('Ctrl Pts',(128.044747647187,5.9188445484099,334.992893055013));
#12125=CARTESIAN_POINT('Ctrl Pts',(128.037350518723,5.91445848589812,334.835344659705));
#12126=CARTESIAN_POINT('Ctrl Pts',(128.029952251287,5.91007174804219,334.677772005876));
#12127=CARTESIAN_POINT('Ctrl Pts',(128.02255398385,5.89938438797449,334.520402674066));
#12128=CARTESIAN_POINT('Ctrl Pts',(128.015155716414,5.88244408076651,334.36377504045));
#12129=CARTESIAN_POINT('Ctrl Pts',(128.007754849888,5.86549782225043,334.207092381898));
#12130=CARTESIAN_POINT('Ctrl Pts',(128.000353983362,5.84229428302207,334.051152311142));
#12131=CARTESIAN_POINT('Ctrl Pts',(127.992953116836,5.81293271448255,333.89648569588));
#12132=CARTESIAN_POINT('Ctrl Pts',(127.985544123452,5.78353890413376,333.741649241887));
#12133=CARTESIAN_POINT('Ctrl Pts',(127.978135130067,5.74797362983715,333.588089402902));
#12134=CARTESIAN_POINT('Ctrl Pts',(127.970726136682,5.70638692576973,333.436325220545));
#12135=CARTESIAN_POINT('Ctrl Pts',(127.963312579102,5.66477460285813,333.284467546217));
#12136=CARTESIAN_POINT('Ctrl Pts',(127.955899021522,5.6171335713578,333.134408087623));
#12137=CARTESIAN_POINT('Ctrl Pts',(127.948485463941,5.56366282881179,332.986647946881));
#12138=CARTESIAN_POINT('Ctrl Pts',(127.941061351805,5.51011596087462,332.838677442528));
#12139=CARTESIAN_POINT('Ctrl Pts',(127.933637239668,5.45072294633833,332.693013138515));
#12140=CARTESIAN_POINT('Ctrl Pts',(127.926213127531,5.3857300639857,332.550134240335));
#12141=CARTESIAN_POINT('Ctrl Pts',(127.922356002377,5.35196364494825,332.475902900333));
#12142=CARTESIAN_POINT('Ctrl Pts',(127.918498877222,5.31668644421776,332.402422977283));
#12143=CARTESIAN_POINT('Ctrl Pts',(127.914641752068,5.27993767406057,332.329758677472));
#12144=CARTESIAN_POINT('Ctrl Pts',(127.90721777463,5.20920570929686,332.189898522375));
#12145=CARTESIAN_POINT('Ctrl Pts',(127.899793797192,5.13280607528259,332.052639748412));
#12146=CARTESIAN_POINT('Ctrl Pts',(127.892369819754,5.05095359418336,331.918474671221));
#12147=CARTESIAN_POINT('Ctrl Pts',(127.884954603726,4.96919771132714,331.784467929008));
#12148=CARTESIAN_POINT('Ctrl Pts',(127.877539387699,4.88200198319752,331.653547931638));
#12149=CARTESIAN_POINT('Ctrl Pts',(127.870124171671,4.78962828222269,331.526184881052));
#12150=CARTESIAN_POINT('Ctrl Pts',(127.862716090527,4.69734346275759,331.398944378551));
#12151=CARTESIAN_POINT('Ctrl Pts',(127.855308009383,4.59989080677096,331.275254309417));
#12152=CARTESIAN_POINT('Ctrl Pts',(127.847899928239,4.497576813013,331.155558119369));
#12153=CARTESIAN_POINT('Ctrl Pts',(127.840497361065,4.39533897342959,331.035951021382));
#12154=CARTESIAN_POINT('Ctrl Pts',(127.833094793891,4.28824724225886,330.920332165847));
#12155=CARTESIAN_POINT('Ctrl Pts',(127.825692226717,4.17664985683644,330.809113872236));
#12156=CARTESIAN_POINT('Ctrl Pts',(127.818293556962,4.06511122695055,330.697954134571));
#12157=CARTESIAN_POINT('Ctrl Pts',(127.810894887207,3.94907193088764,330.591190607421));
#12158=CARTESIAN_POINT('Ctrl Pts',(127.803496217453,3.82891862377498,330.489200432849));
#12159=CARTESIAN_POINT('Ctrl Pts',(127.796098768249,3.70878513822579,330.387227083488));
#12160=CARTESIAN_POINT('Ctrl Pts',(127.788701319045,3.58453927284678,330.290025765144));
#12161=CARTESIAN_POINT('Ctrl Pts',(127.781303869841,3.456602566142,330.197934896085));
#12162=CARTESIAN_POINT('Ctrl Pts',(127.773906741378,3.32867140654993,330.105848019925));
#12163=CARTESIAN_POINT('Ctrl Pts',(127.766509612914,3.1970500267216,330.018871370508));
#12164=CARTESIAN_POINT('Ctrl Pts',(127.759112484451,3.06219066986195,329.93730122722));
#12165=CARTESIAN_POINT('Ctrl Pts',(127.751714217014,2.92731054802768,329.855718524166));
#12166=CARTESIAN_POINT('Ctrl Pts',(127.744315949578,2.78919177580796,329.779544177959));
#12167=CARTESIAN_POINT('Ctrl Pts',(127.736917682141,2.64831288493154,329.709029443854));
#12168=CARTESIAN_POINT('Ctrl Pts',(127.729516815615,2.50738450182041,329.638489937182));
#12169=CARTESIAN_POINT('Ctrl Pts',(127.72211594909,2.36369440299247,329.57361416822));
#12170=CARTESIAN_POINT('Ctrl Pts',(127.714715082564,2.21774271704954,329.51460595732));
#12171=CARTESIAN_POINT('Ctrl Pts',(127.707306089179,2.07163076220076,329.455532949762));
#12172=CARTESIAN_POINT('Ctrl Pts',(127.699897095794,1.92325260688589,329.402340507533));
#12173=CARTESIAN_POINT('Ctrl Pts',(127.69248810241,1.77312591638003,329.355183346896));
#12174=CARTESIAN_POINT('Ctrl Pts',(127.685074544829,1.62290674265451,329.307997135821));
#12175=CARTESIAN_POINT('Ctrl Pts',(127.677660987249,1.47093724675896,329.266853712132));
#12176=CARTESIAN_POINT('Ctrl Pts',(127.670247429669,1.31774650514284,329.231856909656));
#12177=CARTESIAN_POINT('Ctrl Pts',(127.662823317532,1.16433766846065,329.196810282825));
#12178=CARTESIAN_POINT('Ctrl Pts',(127.655399205396,1.00970447946961,329.167927822725));
#12179=CARTESIAN_POINT('Ctrl Pts',(127.647975093259,0.854383187870459,329.145261753863));
#12180=CARTESIAN_POINT('Ctrl Pts',(127.644117968104,0.77368752354308,329.133485818537));
#12181=CARTESIAN_POINT('Ctrl Pts',(127.640260842949,0.692806171097826,329.123386966597));
#12182=CARTESIAN_POINT('Ctrl Pts',(127.636403717794,0.611814342979406,329.114966969317));
#12183=CARTESIAN_POINT('Ctrl Pts',(127.628979740356,0.455925830039553,329.09876063239));
#12184=CARTESIAN_POINT('Ctrl Pts',(127.621555762919,0.299157772951509,329.08872811605));
#12185=CARTESIAN_POINT('Ctrl Pts',(127.614131785481,0.142040423038221,329.084955191994));
#12186=CARTESIAN_POINT('Ctrl Pts',(127.606716569453,-0.0148915047626448,
329.081186720556));
#12187=CARTESIAN_POINT('Ctrl Pts',(127.599301353425,-0.172171535386678,
329.083663145815));
#12188=CARTESIAN_POINT('Ctrl Pts',(127.591886137398,-0.329262551795625,
329.092418706908));
#12189=CARTESIAN_POINT('Ctrl Pts',(127.584478056254,-0.486202416019711,
329.101165843445));
#12190=CARTESIAN_POINT('Ctrl Pts',(127.577069975109,-0.642953257952551,
329.116180067183));
#12191=CARTESIAN_POINT('Ctrl Pts',(127.569661893965,-0.79897631056802,329.137443610706));
#12192=CARTESIAN_POINT('Ctrl Pts',(127.562259326791,-0.954883232375269,
329.158691327386));
#12193=CARTESIAN_POINT('Ctrl Pts',(127.554856759617,-1.1100630752735,329.18617905189));
#12194=CARTESIAN_POINT('Ctrl Pts',(127.547454192443,-1.26398065981757,329.21983707374));
#12195=CARTESIAN_POINT('Ctrl Pts',(127.540055522689,-1.41781720742727,329.253477374789));
#12196=CARTESIAN_POINT('Ctrl Pts',(127.532656852934,-1.57039245654284,329.293281423808));
#12197=CARTESIAN_POINT('Ctrl Pts',(127.525258183179,-1.72118001908107,329.339128167463));
#12198=CARTESIAN_POINT('Ctrl Pts',(127.517860733975,-1.87194270635315,329.384967347828));
#12199=CARTESIAN_POINT('Ctrl Pts',(127.510463284771,-2.02091793563043,329.436847135928));
#12200=CARTESIAN_POINT('Ctrl Pts',(127.503065835567,-2.1675930050995,329.494596188585));
#12201=CARTESIAN_POINT('Ctrl Pts',(127.495668707104,-2.3142617149929,329.552342737344));
#12202=CARTESIAN_POINT('Ctrl Pts',(127.48827157864,-2.45863011611126,329.615957907941));
#12203=CARTESIAN_POINT('Ctrl Pts',(127.480874450177,-2.60020432604942,329.685221733196));
#12204=CARTESIAN_POINT('Ctrl Pts',(127.47347618274,-2.74180033488235,329.754496223351));
#12205=CARTESIAN_POINT('Ctrl Pts',(127.466077915304,-2.8806009606181,329.829420935929));
#12206=CARTESIAN_POINT('Ctrl Pts',(127.458679647867,-3.016135956375,329.909729432028));
#12207=CARTESIAN_POINT('Ctrl Pts',(127.451278781341,-3.15171856700074,329.990066141346));
#12208=CARTESIAN_POINT('Ctrl Pts',(127.443877914815,-3.28403294259744,330.075790209788));
#12209=CARTESIAN_POINT('Ctrl Pts',(127.43647704829,-3.41263703799864,330.166591367432));
#12210=CARTESIAN_POINT('Ctrl Pts',(127.429068054905,-3.54138235299166,330.257492233429));
#12211=CARTESIAN_POINT('Ctrl Pts',(127.42165906152,-3.66640894625044,330.35348110707));
#12212=CARTESIAN_POINT('Ctrl Pts',(127.414250068135,-3.78730657518395,330.454206398431));
#12213=CARTESIAN_POINT('Ctrl Pts',(127.406836510555,-3.90827868122739,330.554993740046));
#12214=CARTESIAN_POINT('Ctrl Pts',(127.399422952975,-4.02511647820144,330.660523063904));
#12215=CARTESIAN_POINT('Ctrl Pts',(127.392009395395,-4.13744633639875,330.770405648774));
#12216=CARTESIAN_POINT('Ctrl Pts',(127.384585283258,-4.24993611671397,330.880444671621));
#12217=CARTESIAN_POINT('Ctrl Pts',(127.377161171121,-4.35790488500537,330.994849062763));
#12218=CARTESIAN_POINT('Ctrl Pts',(127.369737058985,-4.46101852908957,331.113196140063));
#12219=CARTESIAN_POINT('Ctrl Pts',(127.36587993383,-4.51459021861594,331.174682211453));
#12220=CARTESIAN_POINT('Ctrl Pts',(127.362022808675,-4.56685209943981,331.237231997994));
#12221=CARTESIAN_POINT('Ctrl Pts',(127.35816568352,-4.61776198028851,331.300783210475));
#12222=CARTESIAN_POINT('Ctrl Pts',(127.350755590316,-4.71556719711442,331.422874246884));
#12223=CARTESIAN_POINT('Ctrl Pts',(127.343345497113,-4.80868200190314,331.549040297182));
#12224=CARTESIAN_POINT('Ctrl Pts',(127.335935403909,-4.8967462828363,331.678884765018));
#12225=CARTESIAN_POINT('Ctrl Pts',(127.328537236175,-4.98466883708833,331.808520267025));
#12226=CARTESIAN_POINT('Ctrl Pts',(127.32113906844,-5.06755685277397,331.941822085217));
#12227=CARTESIAN_POINT('Ctrl Pts',(127.313740900706,-5.14509003449473,332.07836020368));
#12228=CARTESIAN_POINT('Ctrl Pts',(127.306349693167,-5.22255027301627,332.214769867112));
#12229=CARTESIAN_POINT('Ctrl Pts',(127.298958485627,-5.29466551950669,332.354409448406));
#12230=CARTESIAN_POINT('Ctrl Pts',(127.291567278087,-5.3611580764368,332.49681909524));
#12231=CARTESIAN_POINT('Ctrl Pts',(127.284181551165,-5.42760132880623,332.639123144615));
#12232=CARTESIAN_POINT('Ctrl Pts',(127.276795824242,-5.48843003260356,332.78419283324));
#12233=CARTESIAN_POINT('Ctrl Pts',(127.269410097319,-5.54341193738866,332.931542928916));
#12234=CARTESIAN_POINT('Ctrl Pts',(127.26202837521,-5.59836402896301,333.078813125951));
#12235=CARTESIAN_POINT('Ctrl Pts',(127.2546466531,-5.64747550312645,333.228360918027));
#12236=CARTESIAN_POINT('Ctrl Pts',(127.24726493099,-5.69056192600681,333.379680423873));
#12237=CARTESIAN_POINT('Ctrl Pts',(127.239885009437,-5.73363783920222,333.530963019707));
#12238=CARTESIAN_POINT('Ctrl Pts',(127.232505087885,-5.77069152085042,333.684016110063));
#12239=CARTESIAN_POINT('Ctrl Pts',(127.225125166332,-5.80158817946097,333.838317961558));
#12240=CARTESIAN_POINT('Ctrl Pts',(127.217746325309,-5.83248031434543,333.992597220988));
#12241=CARTESIAN_POINT('Ctrl Pts',(127.210367484285,-5.85721715124729,334.148124509523));
#12242=CARTESIAN_POINT('Ctrl Pts',(127.202988643262,-5.87571493624477,334.304367517657));
#12243=CARTESIAN_POINT('Ctrl Pts',(127.19560781495,-5.894217703114,334.460652605567));
#12244=CARTESIAN_POINT('Ctrl Pts',(127.188226986638,-5.90647801889204,334.617653425809));
#12245=CARTESIAN_POINT('Ctrl Pts',(127.180846158326,-5.91246394690351,334.774831975924));
#12246=CARTESIAN_POINT('Ctrl Pts',(127.177248107118,-5.91538200360392,334.851454334303));
#12247=CARTESIAN_POINT('Ctrl Pts',(127.173650055911,-5.91680978494413,334.928118884487));
#12248=CARTESIAN_POINT('Ctrl Pts',(127.170052004703,-5.91674808267963,335.00476325591));
#12249=CARTESIAN_POINT('',(125.420052711425,-5.92190284584293,335.001236346159));
#12250=CARTESIAN_POINT('Ctrl Pts',(127.170050046356,-5.91164874592261,335.004800830766));
#12251=CARTESIAN_POINT('Ctrl Pts',(127.140009247319,-5.91645495858893,335.644171629641));
#12252=CARTESIAN_POINT('Ctrl Pts',(127.017222436859,-5.5259482387815,338.251773747601));
#12253=CARTESIAN_POINT('Ctrl Pts',(126.801689614972,-1.71899598251946,341.782158633747));
#12254=CARTESIAN_POINT('Ctrl Pts',(126.523451580698,4.77301452401663,340.115755591771));
#12255=CARTESIAN_POINT('Ctrl Pts',(126.245213546424,6.88490005144117,333.754699151657));
#12256=CARTESIAN_POINT('Ctrl Pts',(125.96697551215,2.67861442261645,328.536436919456));
#12257=CARTESIAN_POINT('Ctrl Pts',(125.691922095927,-3.90951754564736,329.241527458829));
#12258=CARTESIAN_POINT('Ctrl Pts',(125.509614691129,-5.92071945294146,333.107089038917));
#12259=CARTESIAN_POINT('Ctrl Pts',(125.420053297756,-5.92617800717982,335.001224849182));
#12260=CARTESIAN_POINT('',(123.670052008058,-5.91563694601309,334.994569125369));
#12261=CARTESIAN_POINT('Ctrl Pts',(125.420052004703,-5.91674986791655,335.001250203804));
#12262=CARTESIAN_POINT('Ctrl Pts',(125.41686781767,-5.91673566116889,335.068485459398));
#12263=CARTESIAN_POINT('Ctrl Pts',(125.413683630636,-5.91557544751366,335.135707266568));
#12264=CARTESIAN_POINT('Ctrl Pts',(125.410499443602,-5.91327036300921,335.202889567147));
#12265=CARTESIAN_POINT('Ctrl Pts',(125.403075466164,-5.90789602564378,335.359526058174));
#12266=CARTESIAN_POINT('Ctrl Pts',(125.395651488726,-5.89628557189547,335.51618515453));
#12267=CARTESIAN_POINT('Ctrl Pts',(125.388227511288,-5.87842692712291,335.672329848345));
#12268=CARTESIAN_POINT('Ctrl Pts',(125.380812295261,-5.86058935823815,335.828290267929));
#12269=CARTESIAN_POINT('Ctrl Pts',(125.373397079233,-5.83651831800253,335.983737126171));
#12270=CARTESIAN_POINT('Ctrl Pts',(125.365981863205,-5.80625371891772,336.138133697794));
#12271=CARTESIAN_POINT('Ctrl Pts',(125.358573782061,-5.77601824027782,336.292381709813));
#12272=CARTESIAN_POINT('Ctrl Pts',(125.351165700917,-5.73960113817575,336.445581083296));
#12273=CARTESIAN_POINT('Ctrl Pts',(125.343757619773,-5.69709406484713,336.597200606932));
#12274=CARTESIAN_POINT('Ctrl Pts',(125.336355052599,-5.65461863030943,336.748707277388));
#12275=CARTESIAN_POINT('Ctrl Pts',(125.328952485425,-5.60606235047825,336.89863608159));
#12276=CARTESIAN_POINT('Ctrl Pts',(125.321549918251,-5.55156783453554,337.046466501326));
#12277=CARTESIAN_POINT('Ctrl Pts',(125.314151248496,-5.49710200971745,337.194219088992));
#12278=CARTESIAN_POINT('Ctrl Pts',(125.306752578742,-5.43670430406923,337.339875143151));
#12279=CARTESIAN_POINT('Ctrl Pts',(125.299353908987,-5.37056697394703,337.482929910579));
#12280=CARTESIAN_POINT('Ctrl Pts',(125.291956459783,-5.30444055443047,337.625961078414));
#12281=CARTESIAN_POINT('Ctrl Pts',(125.284559010579,-5.2325765461144,337.766391472775));
#12282=CARTESIAN_POINT('Ctrl Pts',(125.277161561375,-5.15521513670821,337.90373680914));
#12283=CARTESIAN_POINT('Ctrl Pts',(125.269764432911,-5.07785708155784,338.041076190451));
#12284=CARTESIAN_POINT('Ctrl Pts',(125.262367304448,-4.99500228241028,338.175330454555));
#12285=CARTESIAN_POINT('Ctrl Pts',(125.254970175984,-4.90693650275019,338.306040641081));
#12286=CARTESIAN_POINT('Ctrl Pts',(125.247571908548,-4.81885716315839,338.436770953712));
#12287=CARTESIAN_POINT('Ctrl Pts',(125.240173641111,-4.72556545399591,338.563955792672));
#12288=CARTESIAN_POINT('Ctrl Pts',(125.232775373675,-4.62738992069319,338.687165996313));
#12289=CARTESIAN_POINT('Ctrl Pts',(125.225374507149,-4.52917989729312,338.810419484994));
#12290=CARTESIAN_POINT('Ctrl Pts',(125.217973640623,-4.42608286614893,338.929695266565));
#12291=CARTESIAN_POINT('Ctrl Pts',(125.210572774097,-4.31846691137618,339.044598137992));
#12292=CARTESIAN_POINT('Ctrl Pts',(125.203163780712,-4.21073278399664,339.159627183757));
#12293=CARTESIAN_POINT('Ctrl Pts',(125.195754787328,-4.09847007846341,339.270273457221));
#12294=CARTESIAN_POINT('Ctrl Pts',(125.188345793943,-3.98208343545538,339.376178935507));
#12295=CARTESIAN_POINT('Ctrl Pts',(125.180932236363,-3.86562509426086,339.48214965522));
#12296=CARTESIAN_POINT('Ctrl Pts',(125.173518678782,-3.74503803851658,339.583373520898));
#12297=CARTESIAN_POINT('Ctrl Pts',(125.166105121202,-3.62075865534695,339.679533878735));
#12298=CARTESIAN_POINT('Ctrl Pts',(125.158681009065,-3.4963023377229,339.775831138447));
#12299=CARTESIAN_POINT('Ctrl Pts',(125.151256896929,-3.3681434972203,339.867050277009));
#12300=CARTESIAN_POINT('Ctrl Pts',(125.143832784792,-3.23674672785962,339.952918450993));
#12301=CARTESIAN_POINT('Ctrl Pts',(125.139975659637,-3.16848081605814,339.997530424486));
#12302=CARTESIAN_POINT('Ctrl Pts',(125.136118534483,-3.09934131815225,340.040698813525));
#12303=CARTESIAN_POINT('Ctrl Pts',(125.132261409328,-3.0293957313334,340.082390388929));
#12304=CARTESIAN_POINT('Ctrl Pts',(125.12483743189,-2.89476840200828,340.162635987077));
#12305=CARTESIAN_POINT('Ctrl Pts',(125.117413454452,-2.75674734297633,340.237649734957));
#12306=CARTESIAN_POINT('Ctrl Pts',(125.109989477014,-2.61577760133092,340.307130872974));
#12307=CARTESIAN_POINT('Ctrl Pts',(125.102574260987,-2.4749742251906,340.376530012795));
#12308=CARTESIAN_POINT('Ctrl Pts',(125.095159044959,-2.33122942471442,340.440409376061));
#12309=CARTESIAN_POINT('Ctrl Pts',(125.087743828931,-2.18501614258361,340.498512073202));
#12310=CARTESIAN_POINT('Ctrl Pts',(125.080335747787,-2.03894354613673,340.556558864221));
#12311=CARTESIAN_POINT('Ctrl Pts',(125.072927666643,-1.89040754104931,340.608839917708));
#12312=CARTESIAN_POINT('Ctrl Pts',(125.065519585499,-1.73990443252952,340.655144837063));
#12313=CARTESIAN_POINT('Ctrl Pts',(125.058117018325,-1.58951334622209,340.701415290822));
#12314=CARTESIAN_POINT('Ctrl Pts',(125.050714451151,-1.43715842700227,340.741718358076));
#12315=CARTESIAN_POINT('Ctrl Pts',(125.043311883977,-1.2833545637519,340.775892279657));
#12316=CARTESIAN_POINT('Ctrl Pts',(125.035913214222,-1.12963167756334,340.810048208817));
#12317=CARTESIAN_POINT('Ctrl Pts',(125.028514544468,-0.974461730039377,
340.838081338257));
#12318=CARTESIAN_POINT('Ctrl Pts',(125.021115874713,-0.818373219880692,
340.859880189516));
#12319=CARTESIAN_POINT('Ctrl Pts',(125.013718425509,-0.662310459479376,
340.881675444641));
#12320=CARTESIAN_POINT('Ctrl Pts',(125.006320976305,-0.505329806454695,
340.89723841118));
#12321=CARTESIAN_POINT('Ctrl Pts',(124.998923527101,-0.347968485344661,
340.906508993958));
#12322=CARTESIAN_POINT('Ctrl Pts',(124.991526398637,-0.190613987147168,
340.91577917478));
#12323=CARTESIAN_POINT('Ctrl Pts',(124.984129270174,-0.0328792262472288,
340.918757492362));
#12324=CARTESIAN_POINT('Ctrl Pts',(124.976732141711,0.1246952047689,340.915435881523));
#12325=CARTESIAN_POINT('Ctrl Pts',(124.969333874274,0.282293898313986,340.912113759239));
#12326=CARTESIAN_POINT('Ctrl Pts',(124.961935606837,0.439731839669498,340.902489784938));
#12327=CARTESIAN_POINT('Ctrl Pts',(124.954537339401,0.596470342866343,340.886607995491));
#12328=CARTESIAN_POINT('Ctrl Pts',(124.947136472875,0.753263909947715,340.870720626604));
#12329=CARTESIAN_POINT('Ctrl Pts',(124.939735606349,0.909357178566269,340.848571103088));
#12330=CARTESIAN_POINT('Ctrl Pts',(124.932334739823,1.06421862262364,340.820255087688));
#12331=CARTESIAN_POINT('Ctrl Pts',(124.924925746439,1.21925011935187,340.791907978597));
#12332=CARTESIAN_POINT('Ctrl Pts',(124.917516753054,1.37304672283874,340.757380921947));
#12333=CARTESIAN_POINT('Ctrl Pts',(124.910107759669,1.52508838971938,340.716820441998));
#12334=CARTESIAN_POINT('Ctrl Pts',(124.902694202089,1.67722371951129,340.676234975393));
#12335=CARTESIAN_POINT('Ctrl Pts',(124.895280644509,1.82760160282278,340.629608789548));
#12336=CARTESIAN_POINT('Ctrl Pts',(124.887867086929,1.97571960460233,340.577137492163));
#12337=CARTESIAN_POINT('Ctrl Pts',(124.880442974792,2.124048479474,340.52459149228));
#12338=CARTESIAN_POINT('Ctrl Pts',(124.873018862655,2.27011070151455,340.466183899181));
#12339=CARTESIAN_POINT('Ctrl Pts',(124.865594750518,2.413425412381,340.402157748657));
#12340=CARTESIAN_POINT('Ctrl Pts',(124.861737625364,2.48788317462133,340.368893585724));
#12341=CARTESIAN_POINT('Ctrl Pts',(124.857880500209,2.56159974346398,340.334113599218));
#12342=CARTESIAN_POINT('Ctrl Pts',(124.854023375054,2.63451064917932,340.29785656675));
#12343=CARTESIAN_POINT('Ctrl Pts',(124.846599397616,2.77484545743852,340.228071071022));
#12344=CARTESIAN_POINT('Ctrl Pts',(124.839175420178,2.91261723306796,340.152600461198));
#12345=CARTESIAN_POINT('Ctrl Pts',(124.83175144274,3.04733222038819,340.071656228599));
#12346=CARTESIAN_POINT('Ctrl Pts',(124.824336226713,3.18188822375451,339.990807522373));
#12347=CARTESIAN_POINT('Ctrl Pts',(124.816921010685,3.31339430274406,339.904498241852));
#12348=CARTESIAN_POINT('Ctrl Pts',(124.809505794658,3.44137849701398,339.81298707694));
#12349=CARTESIAN_POINT('Ctrl Pts',(124.802097713513,3.56923954553658,339.72156396361));
#12350=CARTESIAN_POINT('Ctrl Pts',(124.794689632369,3.69358515412853,339.624949145983));
#12351=CARTESIAN_POINT('Ctrl Pts',(124.787281551225,3.81396981657318,339.523446120025));
#12352=CARTESIAN_POINT('Ctrl Pts',(124.779878984051,3.93426487451491,339.422018644623));
#12353=CARTESIAN_POINT('Ctrl Pts',(124.772476416877,4.05060457251039,339.315710444982));
#12354=CARTESIAN_POINT('Ctrl Pts',(124.765073849703,4.16257424790502,339.20486696498));
#12355=CARTESIAN_POINT('Ctrl Pts',(124.757675179949,4.27448497175487,339.094081843586));
#12356=CARTESIAN_POINT('Ctrl Pts',(124.750276510194,4.38202999061649,338.978766459188));
#12357=CARTESIAN_POINT('Ctrl Pts',(124.742877840439,4.48482955890165,338.859304910227));
#12358=CARTESIAN_POINT('Ctrl Pts',(124.735480391235,4.58761216845022,338.739863068712));
#12359=CARTESIAN_POINT('Ctrl Pts',(124.728082942031,4.68565063793362,338.616276702745));
#12360=CARTESIAN_POINT('Ctrl Pts',(124.720685492827,4.77860370901436,338.488965054955));
#12361=CARTESIAN_POINT('Ctrl Pts',(124.713288364364,4.87155274981196,338.361658927175));
#12362=CARTESIAN_POINT('Ctrl Pts',(124.7058912359,4.95941661054792,338.23062814015));
#12363=CARTESIAN_POINT('Ctrl Pts',(124.698494107437,5.04189596337167,338.096322925187));
#12364=CARTESIAN_POINT('Ctrl Pts',(124.69109584,5.12438801595684,337.961997030573));
#12365=CARTESIAN_POINT('Ctrl Pts',(124.683697572563,5.20149371450388,337.824396022178));
#12366=CARTESIAN_POINT('Ctrl Pts',(124.676299305127,5.2729585766679,337.683996723404));
#12367=CARTESIAN_POINT('Ctrl Pts',(124.668898438601,5.34444854518958,337.54354810088));
#12368=CARTESIAN_POINT('Ctrl Pts',(124.661497572075,5.41029356260449,337.40029956308));
#12369=CARTESIAN_POINT('Ctrl Pts',(124.65409670555,5.47028643448658,337.254749850243));
#12370=CARTESIAN_POINT('Ctrl Pts',(124.646687712165,5.53034518427751,337.109040309906));
#12371=CARTESIAN_POINT('Ctrl Pts',(124.63927871878,5.58453881273266,336.961024893413));
#12372=CARTESIAN_POINT('Ctrl Pts',(124.631869725395,5.63270910992128,336.811220209005));
#12373=CARTESIAN_POINT('Ctrl Pts',(124.624456167815,5.68090908167455,336.661323239745));
#12374=CARTESIAN_POINT('Ctrl Pts',(124.617042610235,5.72307822861242,336.509635164927));
#12375=CARTESIAN_POINT('Ctrl Pts',(124.609629052655,5.75910914498714,336.356684347454));
#12376=CARTESIAN_POINT('Ctrl Pts',(124.602204940518,5.79519135796764,336.203515776491));
#12377=CARTESIAN_POINT('Ctrl Pts',(124.594780828381,5.82511781625476,336.049081237823));
#12378=CARTESIAN_POINT('Ctrl Pts',(124.587356716244,5.84883267378686,335.893916616102));
#12379=CARTESIAN_POINT('Ctrl Pts',(124.58349959109,5.86115349705078,335.813302348087));
#12380=CARTESIAN_POINT('Ctrl Pts',(124.579642465935,5.87179852965587,335.732491066298));
#12381=CARTESIAN_POINT('Ctrl Pts',(124.57578534078,5.88076549225369,335.651557969499));
#12382=CARTESIAN_POINT('Ctrl Pts',(124.568361363342,5.89802459724597,335.495782499293));
#12383=CARTESIAN_POINT('Ctrl Pts',(124.560937385904,5.90911596448591,335.339085796455));
#12384=CARTESIAN_POINT('Ctrl Pts',(124.553513408466,5.9139502420072,335.181997520761));
#12385=CARTESIAN_POINT('Ctrl Pts',(124.546098192439,5.91877881435365,335.025094632867));
#12386=CARTESIAN_POINT('Ctrl Pts',(124.538682976411,5.91736498419445,334.86780146137));
#12387=CARTESIAN_POINT('Ctrl Pts',(124.531267760383,5.90967088456563,334.710654879742));
#12388=CARTESIAN_POINT('Ctrl Pts',(124.523859679239,5.90198418816074,334.553659503763));
#12389=CARTESIAN_POINT('Ctrl Pts',(124.516451598095,5.88802927059053,334.396810807126));
#12390=CARTESIAN_POINT('Ctrl Pts',(124.509043516951,5.86782025910927,334.240647664594));
#12391=CARTESIAN_POINT('Ctrl Pts',(124.501640949777,5.84762628956434,334.08460075714));
#12392=CARTESIAN_POINT('Ctrl Pts',(124.494238382603,5.82118754265617,333.929238756309));
#12393=CARTESIAN_POINT('Ctrl Pts',(124.486835815429,5.78857011175512,333.775097300274));
#12394=CARTESIAN_POINT('Ctrl Pts',(124.479437145674,5.75596985378888,333.621036999043));
#12395=CARTESIAN_POINT('Ctrl Pts',(124.47203847592,5.71719746754077,333.468196327017));
#12396=CARTESIAN_POINT('Ctrl Pts',(124.464639806165,5.67237044745629,333.317102478068));
#12397=CARTESIAN_POINT('Ctrl Pts',(124.457242356961,5.62755082243814,333.166033554913));
#12398=CARTESIAN_POINT('Ctrl Pts',(124.449844907757,5.57667865198069,333.016711240356));
#12399=CARTESIAN_POINT('Ctrl Pts',(124.442447458553,5.51992181168633,332.869649382057));
#12400=CARTESIAN_POINT('Ctrl Pts',(124.435050330089,5.46316743226963,332.722593900104));
#12401=CARTESIAN_POINT('Ctrl Pts',(124.427653201626,5.40052902471263,332.577799027714));
#12402=CARTESIAN_POINT('Ctrl Pts',(124.420256073163,5.33222321465083,332.435760122056));
#12403=CARTESIAN_POINT('Ctrl Pts',(124.412857805726,5.2639068871994,332.293699345952));
#12404=CARTESIAN_POINT('Ctrl Pts',(124.405459538289,5.18992158145961,332.15439571788));
#12405=CARTESIAN_POINT('Ctrl Pts',(124.398061270853,5.11053055340252,332.018321273973));
#12406=CARTESIAN_POINT('Ctrl Pts',(124.390660404327,5.03111163444238,331.882199025684));
#12407=CARTESIAN_POINT('Ctrl Pts',(124.383259537801,4.94628340004286,331.749308542395));
#12408=CARTESIAN_POINT('Ctrl Pts',(124.375858671275,4.85635312671682,331.620093955281));
#12409=CARTESIAN_POINT('Ctrl Pts',(124.368449677891,4.76632410135291,331.490737478197));
#12410=CARTESIAN_POINT('Ctrl Pts',(124.361040684506,4.67118206183956,331.365065264871));
#12411=CARTESIAN_POINT('Ctrl Pts',(124.353631691121,4.57127581859846,331.243489923773));
#12412=CARTESIAN_POINT('Ctrl Pts',(124.346218133541,4.47130802966539,331.121839688071));
#12413=CARTESIAN_POINT('Ctrl Pts',(124.338804575961,4.36657043650021,331.004291631627));
#12414=CARTESIAN_POINT('Ctrl Pts',(124.33139101838,4.2574492273283,330.891222001711));
#12415=CARTESIAN_POINT('Ctrl Pts',(124.323966906244,4.14817266413791,330.777991396477));
#12416=CARTESIAN_POINT('Ctrl Pts',(124.316542794107,4.03450028961519,330.669252208925));
#12417=CARTESIAN_POINT('Ctrl Pts',(124.30911868197,3.91685251908634,330.565341399135));
#12418=CARTESIAN_POINT('Ctrl Pts',(124.305261556816,3.85572976571972,330.511355549931));
#12419=CARTESIAN_POINT('Ctrl Pts',(124.301404431661,3.79353447278618,330.458672293386));
#12420=CARTESIAN_POINT('Ctrl Pts',(124.297547306506,3.73032864304282,330.407334240619));
#12421=CARTESIAN_POINT('Ctrl Pts',(124.290123329068,3.60867361886075,330.3085216457));
#12422=CARTESIAN_POINT('Ctrl Pts',(124.28269935163,3.48290619370343,330.214397101204));
#12423=CARTESIAN_POINT('Ctrl Pts',(124.275275374192,3.35342341629837,330.1253223744));
#12424=CARTESIAN_POINT('Ctrl Pts',(124.267860158165,3.22409344805238,330.036352769176));
#12425=CARTESIAN_POINT('Ctrl Pts',(124.260444942137,3.0910571598136,329.952421328543));
#12426=CARTESIAN_POINT('Ctrl Pts',(124.25302972611,2.95474552795087,329.873850428679));
#12427=CARTESIAN_POINT('Ctrl Pts',(124.245621644965,2.81856505445383,329.79535512934));
#12428=CARTESIAN_POINT('Ctrl Pts',(124.238213563821,2.67911583260145,329.722210287513));
#12429=CARTESIAN_POINT('Ctrl Pts',(124.230805482677,2.53685865874616,329.654695639344));
#12430=CARTESIAN_POINT('Ctrl Pts',(124.223402915503,2.39470736950351,329.587231243561));
#12431=CARTESIAN_POINT('Ctrl Pts',(124.216000348329,2.24975262549413,329.525388856563));
#12432=CARTESIAN_POINT('Ctrl Pts',(124.208597781155,2.10248062320287,329.469402763575));
#12433=CARTESIAN_POINT('Ctrl Pts',(124.201199111401,1.95528615897728,329.41344614702));
#12434=CARTESIAN_POINT('Ctrl Pts',(124.193800441646,1.8057772142,329.363339816159));
#12435=CARTESIAN_POINT('Ctrl Pts',(124.186401771891,1.65446070043183,329.319270262262));
#12436=CARTESIAN_POINT('Ctrl Pts',(124.179004322687,1.5031691491897,329.275207978472));
#12437=CARTESIAN_POINT('Ctrl Pts',(124.171606873483,1.35007097874838,329.2371805994));
#12438=CARTESIAN_POINT('Ctrl Pts',(124.164209424279,1.19568914168764,329.205325027325));
#12439=CARTESIAN_POINT('Ctrl Pts',(124.156812295816,1.04131399835427,329.173470836451));
#12440=CARTESIAN_POINT('Ctrl Pts',(124.149415167352,0.885655664578183,329.147787995919));
#12441=CARTESIAN_POINT('Ctrl Pts',(124.142018038889,0.729247925332657,329.128362406798));
#12442=CARTESIAN_POINT('Ctrl Pts',(124.134619771452,0.572816103199749,329.108933826622));
#12443=CARTESIAN_POINT('Ctrl Pts',(124.127221504016,0.415635016229508,329.095764462235));
#12444=CARTESIAN_POINT('Ctrl Pts',(124.119823236579,0.258244072589957,329.088888381914));
#12445=CARTESIAN_POINT('Ctrl Pts',(124.112422370053,0.100797835856634,329.082009885953));
#12446=CARTESIAN_POINT('Ctrl Pts',(124.105021503527,-0.0568580317113297,
329.081429092229));
#12447=CARTESIAN_POINT('Ctrl Pts',(124.097620637002,-0.214183765782614,
329.087127950228));
#12448=CARTESIAN_POINT('Ctrl Pts',(124.090211643617,-0.371682258550953,
329.092833066118));
#12449=CARTESIAN_POINT('Ctrl Pts',(124.082802650232,-0.528849520665383,
329.10483159121));
#12450=CARTESIAN_POINT('Ctrl Pts',(124.075393656847,-0.685149819527369,
329.123053489498));
#12451=CARTESIAN_POINT('Ctrl Pts',(124.067980099267,-0.841546404764826,
329.141286613104));
#12452=CARTESIAN_POINT('Ctrl Pts',(124.060566541687,-0.997074594709493,
329.165750691427));
#12453=CARTESIAN_POINT('Ctrl Pts',(124.053152984107,-1.15120900639713,329.196324579537));
#12454=CARTESIAN_POINT('Ctrl Pts',(124.04572887197,-1.30556285663778,329.226941995173));
#12455=CARTESIAN_POINT('Ctrl Pts',(124.038304759833,-1.45851860367209,329.263686506166));
#12456=CARTESIAN_POINT('Ctrl Pts',(124.030880647697,-1.60956537972557,329.30638692473));
#12457=CARTESIAN_POINT('Ctrl Pts',(124.027023522542,-1.6880402611301,329.328571511321));
#12458=CARTESIAN_POINT('Ctrl Pts',(124.023166397387,-1.76600017727977,329.352362926947));
#12459=CARTESIAN_POINT('Ctrl Pts',(124.019309272232,-1.84337574232694,329.377732091487));
#12460=CARTESIAN_POINT('Ctrl Pts',(124.011885294794,-1.99230387561708,329.426561231742));
#12461=CARTESIAN_POINT('Ctrl Pts',(124.004461317356,-2.13951518342932,329.481385550795));
#12462=CARTESIAN_POINT('Ctrl Pts',(123.997037339918,-2.28449058209917,329.542066934929));
#12463=CARTESIAN_POINT('Ctrl Pts',(123.989622123891,-2.42929488798597,329.602676705899));
#12464=CARTESIAN_POINT('Ctrl Pts',(123.982206907863,-2.5718681962005,329.669129640372));
#12465=CARTESIAN_POINT('Ctrl Pts',(123.974791691835,-2.71170618769361,329.741237777373));
#12466=CARTESIAN_POINT('Ctrl Pts',(123.967383610691,-2.8514096277751,329.813276532288));
#12467=CARTESIAN_POINT('Ctrl Pts',(123.959975529547,-2.98838266128292,329.890959487));
#12468=CARTESIAN_POINT('Ctrl Pts',(123.952567448403,-3.12214068877773,329.974050529305));
#12469=CARTESIAN_POINT('Ctrl Pts',(123.945164881229,-3.2557991577301,330.05707972543));
#12470=CARTESIAN_POINT('Ctrl Pts',(123.937762314055,-3.38624706979218,330.145508798021));
#12471=CARTESIAN_POINT('Ctrl Pts',(123.930359746881,-3.5130243007025,330.239055679261));
#12472=CARTESIAN_POINT('Ctrl Pts',(123.922961077126,-3.63973478395483,330.332553308477));
#12473=CARTESIAN_POINT('Ctrl Pts',(123.915562407372,-3.76277813538804,330.431163159045));
#12474=CARTESIAN_POINT('Ctrl Pts',(123.908163737617,-3.88172321158337,330.534559879345));
#12475=CARTESIAN_POINT('Ctrl Pts',(123.900766288413,-4.00064866553452,330.637939542397));
#12476=CARTESIAN_POINT('Ctrl Pts',(123.893368839209,-4.11547690467132,330.746104263301));
#12477=CARTESIAN_POINT('Ctrl Pts',(123.885971390005,-4.22580980530027,330.858688365756));
#12478=CARTESIAN_POINT('Ctrl Pts',(123.878574261541,-4.33613792208701,330.971267586759));
#12479=CARTESIAN_POINT('Ctrl Pts',(123.871177133078,-4.44197082668943,331.088265541764));
#12480=CARTESIAN_POINT('Ctrl Pts',(123.863780004614,-4.54294742138782,331.209279845596));
#12481=CARTESIAN_POINT('Ctrl Pts',(123.856381737178,-4.64393956396104,331.330312782609));
#12482=CARTESIAN_POINT('Ctrl Pts',(123.848983469741,-4.74007366863847,331.455363013227));
#12483=CARTESIAN_POINT('Ctrl Pts',(123.841585202305,-4.83102918196927,331.583995373911));
#12484=CARTESIAN_POINT('Ctrl Pts',(123.834184335779,-4.92201664892828,331.712672924496));
#12485=CARTESIAN_POINT('Ctrl Pts',(123.826783469253,-5.00782168699438,331.844934806164));
#12486=CARTESIAN_POINT('Ctrl Pts',(123.819382602727,-5.08816737777776,331.980317351406));
#12487=CARTESIAN_POINT('Ctrl Pts',(123.811973609343,-5.16860129581119,332.115848559626));
#12488=CARTESIAN_POINT('Ctrl Pts',(123.804564615958,-5.2435637038695,332.254506953758));
#12489=CARTESIAN_POINT('Ctrl Pts',(123.797155622573,-5.31282358107555,332.395804124328));
#12490=CARTESIAN_POINT('Ctrl Pts',(123.789742064993,-5.38212612475491,332.537188338829));
#12491=CARTESIAN_POINT('Ctrl Pts',(123.782328507413,-5.44571898715927,332.681214228331));
#12492=CARTESIAN_POINT('Ctrl Pts',(123.774914949832,-5.50341972677719,332.827374428619));
#12493=CARTESIAN_POINT('Ctrl Pts',(123.767490837696,-5.5612026139615,332.97374271471));
#12494=CARTESIAN_POINT('Ctrl Pts',(123.760066725559,-5.61307650207728,333.122251028857));
#12495=CARTESIAN_POINT('Ctrl Pts',(123.752642613422,-5.65890888671798,333.272377131917));
#12496=CARTESIAN_POINT('Ctrl Pts',(123.748785488268,-5.68272065578047,333.350373686631));
#12497=CARTESIAN_POINT('Ctrl Pts',(123.744928363113,-5.70490253077992,333.428806743467));
#12498=CARTESIAN_POINT('Ctrl Pts',(123.741071237958,-5.72544141714638,333.507602217462));
#12499=CARTESIAN_POINT('Ctrl Pts',(123.731427427444,-5.77679394535045,333.704611282535));
#12500=CARTESIAN_POINT('Ctrl Pts',(123.72178361693,-5.81799862666432,333.904366729355));
#12501=CARTESIAN_POINT('Ctrl Pts',(123.712139806416,-5.84881392545219,334.105960723493));
#12502=CARTESIAN_POINT('Ctrl Pts',(123.702686240882,-5.87902132595345,334.303577840936));
#12503=CARTESIAN_POINT('Ctrl Pts',(123.693232675347,-5.89924525418592,334.502961900108));
#12504=CARTESIAN_POINT('Ctrl Pts',(123.683779109812,-5.90930297922068,334.703236015875));
#12505=CARTESIAN_POINT('Ctrl Pts',(123.67920341457,-5.91417109849555,334.80017227928));
#12506=CARTESIAN_POINT('Ctrl Pts',(123.674627719327,-5.91665821897587,334.897316710721));
#12507=CARTESIAN_POINT('Ctrl Pts',(123.670052024084,-5.91674750630152,334.994567765212));
#12508=CARTESIAN_POINT('',(121.920052004703,-5.90729175175101,335.001447065376));
#12509=CARTESIAN_POINT('Ctrl Pts',(123.670052004703,-5.91540447174683,334.994569410092));
#12510=CARTESIAN_POINT('Ctrl Pts',(123.600979071031,-5.90216581006969,336.462314046667));
#12511=CARTESIAN_POINT('Ctrl Pts',(123.439160125933,-4.60789812849357,339.921680871558));
#12512=CARTESIAN_POINT('Ctrl Pts',(123.18459516941,1.19876002868579,341.893155831318));
#12513=CARTESIAN_POINT('Ctrl Pts',(122.906357135138,6.44531963394435,337.722219266979));
#12514=CARTESIAN_POINT('Ctrl Pts',(122.628119100863,5.77710454389356,331.053142261224));
#12515=CARTESIAN_POINT('Ctrl Pts',(122.34988106659,-0.192674116164957,328.006038346818));
#12516=CARTESIAN_POINT('Ctrl Pts',(122.113858701203,-5.10670098453427,330.865701816946));
#12517=CARTESIAN_POINT('Ctrl Pts',(121.970582347241,-5.90494040890748,333.923998790854));
#12518=CARTESIAN_POINT('Ctrl Pts',(121.920052004703,-5.90729175175101,335.001447065376));
#12519=CARTESIAN_POINT('',(120.170052004703,-5.92072775613925,335.004842343689));
#12520=CARTESIAN_POINT('Ctrl Pts',(121.920052004703,-5.90729175175101,335.001447065376));
#12521=CARTESIAN_POINT('Ctrl Pts',(121.877836335816,-5.90925618551375,335.901603235247));
#12522=CARTESIAN_POINT('Ctrl Pts',(121.742874655505,-5.29259387067636,338.776810722794));
#12523=CARTESIAN_POINT('Ctrl Pts',(121.515166963767,-0.817435776173097,
341.948699279223));
#12524=CARTESIAN_POINT('Ctrl Pts',(121.236928929494,5.40094806495304,339.447739079677));
#12525=CARTESIAN_POINT('Ctrl Pts',(120.958690895219,6.66296158473417,332.865154375237));
#12526=CARTESIAN_POINT('Ctrl Pts',(120.680452860945,1.81047360335528,328.241685990367));
#12527=CARTESIAN_POINT('Ctrl Pts',(120.417573230773,-4.34389803797753,329.733089300436));
#12528=CARTESIAN_POINT('Ctrl Pts',(120.247439612026,-5.90621016686413,333.364210861679));
#12529=CARTESIAN_POINT('Ctrl Pts',(120.170052004703,-5.92072775613925,335.004842343689));
#12530=CARTESIAN_POINT('',(118.420052004704,-5.92029571450889,334.995996540637));
#12531=CARTESIAN_POINT('Ctrl Pts',(120.170052004703,-5.92072775613925,335.004842343689));
#12532=CARTESIAN_POINT('Ctrl Pts',(120.154693600602,-5.92360892807864,335.330443330137));
#12533=CARTESIAN_POINT('Ctrl Pts',(120.046589185076,-5.75090023104754,337.619217809614));
#12534=CARTESIAN_POINT('Ctrl Pts',(119.845738758123,-2.76569986880471,341.426782021898));
#12535=CARTESIAN_POINT('Ctrl Pts',(119.56750072385,3.90773921675531,340.803636544015));
#12536=CARTESIAN_POINT('Ctrl Pts',(119.289262689575,6.99510370123495,334.854579471234));
#12537=CARTESIAN_POINT('Ctrl Pts',(119.011024655301,3.66316476665284,329.038972671294));
#12538=CARTESIAN_POINT('Ctrl Pts',(118.732786621027,-3.03040640606552,328.69371266629));
#12539=CARTESIAN_POINT('Ctrl Pts',(118.535795737496,-5.80051253301409,332.546564672477));
#12540=CARTESIAN_POINT('Ctrl Pts',(118.431550865387,-5.92485583227999,334.752456411305));
#12541=CARTESIAN_POINT('Ctrl Pts',(118.420052004704,-5.92296503915713,334.99599473557));
#12542=CARTESIAN_POINT('',(116.670052030361,-5.91201473463796,334.997295449063));
#12543=CARTESIAN_POINT('Ctrl Pts',(118.420052004704,-5.91674864718901,334.995998939257));
#12544=CARTESIAN_POINT('Ctrl Pts',(118.412737522599,-5.91685329486301,335.150751397025));
#12545=CARTESIAN_POINT('Ctrl Pts',(118.405423040495,-5.9108824720153,335.305741900391));
#12546=CARTESIAN_POINT('Ctrl Pts',(118.39810855839,-5.89880667231961,335.460445876404));
#12547=CARTESIAN_POINT('Ctrl Pts',(118.390801550831,-5.88674321268076,335.614991763023));
#12548=CARTESIAN_POINT('Ctrl Pts',(118.383494543273,-5.86858721879641,335.769251324649));
#12549=CARTESIAN_POINT('Ctrl Pts',(118.376187535715,-5.8443611934897,335.92269865207));
#12550=CARTESIAN_POINT('Ctrl Pts',(118.368886296861,-5.82015429403843,336.076024836573));
#12551=CARTESIAN_POINT('Ctrl Pts',(118.361585058006,-5.7898869595669,336.228539685085));
#12552=CARTESIAN_POINT('Ctrl Pts',(118.354283819152,-5.75363359786507,336.379721342887));
#12553=CARTESIAN_POINT('Ctrl Pts',(118.346868266374,-5.7168126250895,336.533270019335));
#12554=CARTESIAN_POINT('Ctrl Pts',(118.339452713596,-5.67381663270208,336.685443005712));
#12555=CARTESIAN_POINT('Ctrl Pts',(118.332037160818,-5.62477790671428,336.835702607352));
#12556=CARTESIAN_POINT('Ctrl Pts',(118.3247414092,-5.57653142055384,336.983534706269));
#12557=CARTESIAN_POINT('Ctrl Pts',(118.317445657582,-5.52243611057192,337.129514403159));
#12558=CARTESIAN_POINT('Ctrl Pts',(118.310149905963,-5.4626684853699,337.273143986079));
#12559=CARTESIAN_POINT('Ctrl Pts',(118.302854458138,-5.40290334887101,337.416767588312));
#12560=CARTESIAN_POINT('Ctrl Pts',(118.295559010312,-5.33746651456023,337.558040916098));
#12561=CARTESIAN_POINT('Ctrl Pts',(118.288263562487,-5.26658273076751,337.696486028609));
#12562=CARTESIAN_POINT('Ctrl Pts',(118.280966884809,-5.19568699752291,337.83495447993));
#12563=CARTESIAN_POINT('Ctrl Pts',(118.273670207131,-5.11934266325419,337.970593425154));
#12564=CARTESIAN_POINT('Ctrl Pts',(118.266373529452,-5.0378203929602,338.102949604936));
#12565=CARTESIAN_POINT('Ctrl Pts',(118.258868281371,-4.95396786586801,338.239089093091));
#12566=CARTESIAN_POINT('Ctrl Pts',(118.25136303329,-4.8646371873369,338.371754966557));
#12567=CARTESIAN_POINT('Ctrl Pts',(118.243857785209,-4.77017002033784,338.500486900357));
#12568=CARTESIAN_POINT('Ctrl Pts',(118.236550322751,-4.67819234432372,338.625826364595));
#12569=CARTESIAN_POINT('Ctrl Pts',(118.229242860292,-4.58134578891141,338.747436362512));
#12570=CARTESIAN_POINT('Ctrl Pts',(118.221935397834,-4.47998546807229,338.864927006861));
#12571=CARTESIAN_POINT('Ctrl Pts',(118.214331256942,-4.37450998120765,338.987187698344));
#12572=CARTESIAN_POINT('Ctrl Pts',(118.206727116049,-4.26414685358599,339.104987186631));
#12573=CARTESIAN_POINT('Ctrl Pts',(118.199122975157,-4.1493364253379,339.217930510554));
#12574=CARTESIAN_POINT('Ctrl Pts',(118.191518834265,-4.03452599708985,339.330873834477));
#12575=CARTESIAN_POINT('Ctrl Pts',(118.183914693372,-3.91526865943968,339.438960739679));
#12576=CARTESIAN_POINT('Ctrl Pts',(118.17631055248,-3.79204017945385,339.541845642457));
#12577=CARTESIAN_POINT('Ctrl Pts',(118.168886575042,-3.6717313282521,339.642292912932));
#12578=CARTESIAN_POINT('Ctrl Pts',(118.161462597604,-3.54724711066077,339.738108124031));
#12579=CARTESIAN_POINT('Ctrl Pts',(118.154038620166,-3.41897965128562,339.828924176936));
#12580=CARTESIAN_POINT('Ctrl Pts',(118.146623404138,-3.29086356681131,339.919633053234));
#12581=CARTESIAN_POINT('Ctrl Pts',(118.139208188111,-3.15897342943008,340.00535430134));
#12582=CARTESIAN_POINT('Ctrl Pts',(118.131792972083,-3.0237358205097,340.085759751528));
#12583=CARTESIAN_POINT('Ctrl Pts',(118.124384890939,-2.88862833653579,340.166087835998));
#12584=CARTESIAN_POINT('Ctrl Pts',(118.116976809795,-2.7501801119254,340.241110115777));
#12585=CARTESIAN_POINT('Ctrl Pts',(118.109568728651,-2.60884812142239,340.310540654383));
#12586=CARTESIAN_POINT('Ctrl Pts',(118.102166161477,-2.46762132690085,340.37991951457));
#12587=CARTESIAN_POINT('Ctrl Pts',(118.094763594303,-2.32351537389913,340.443714756949));
#12588=CARTESIAN_POINT('Ctrl Pts',(118.087361027129,-2.17701324906763,340.501685548619));
#12589=CARTESIAN_POINT('Ctrl Pts',(118.079962357374,-2.03058825696489,340.559625818921));
#12590=CARTESIAN_POINT('Ctrl Pts',(118.072563687619,-1.88176995168808,340.611747608753));
#12591=CARTESIAN_POINT('Ctrl Pts',(118.065165017865,-1.73106267882237,340.657857594928));
#12592=CARTESIAN_POINT('Ctrl Pts',(118.057767568661,-1.58038026797693,340.703959974388));
#12593=CARTESIAN_POINT('Ctrl Pts',(118.050370119457,-1.42780986454369,340.744052409432));
#12594=CARTESIAN_POINT('Ctrl Pts',(118.042972670253,-1.27387252366521,340.777990944606));
#12595=CARTESIAN_POINT('Ctrl Pts',(118.035575541789,-1.1199418572414,340.811928008265));
#12596=CARTESIAN_POINT('Ctrl Pts',(118.028178413326,-0.964644735675487,
340.839711622233));
#12597=CARTESIAN_POINT('Ctrl Pts',(118.020781284862,-0.808513734597942,
340.861248681251));
#12598=CARTESIAN_POINT('Ctrl Pts',(118.013383017426,-0.652358693243784,
340.882789056439));
#12599=CARTESIAN_POINT('Ctrl Pts',(118.005984749989,-0.495369886456328,
340.898080910577));
#12600=CARTESIAN_POINT('Ctrl Pts',(117.998586482553,-0.338086212866381,
340.907082890494));
#12601=CARTESIAN_POINT('Ctrl Pts',(117.991185616027,-0.180747283867814,
340.916088032902));
#12602=CARTESIAN_POINT('Ctrl Pts',(117.983784749501,-0.0231136541863968,
340.918798880269));
#12603=CARTESIAN_POINT('Ctrl Pts',(117.976383882975,0.134274717233284,340.915226188643));
#12604=CARTESIAN_POINT('Ctrl Pts',(117.968974889591,0.29183591613176,340.911649573861));
#12605=CARTESIAN_POINT('Ctrl Pts',(117.961565896206,0.44915094559031,340.901775649038));
#12606=CARTESIAN_POINT('Ctrl Pts',(117.954156902821,0.6056831756471,340.885667205444));
#12607=CARTESIAN_POINT('Ctrl Pts',(117.946743345241,0.762311834956978,340.869548838493));
#12608=CARTESIAN_POINT('Ctrl Pts',(117.939329787661,0.918156365390284,340.847188352593));
#12609=CARTESIAN_POINT('Ctrl Pts',(117.931916230081,1.0726897951362,340.818699783105));
#12610=CARTESIAN_POINT('Ctrl Pts',(117.924492117944,1.22744323151049,340.790170654924));
#12611=CARTESIAN_POINT('Ctrl Pts',(117.917068005807,1.38088147619017,340.75549610073));
#12612=CARTESIAN_POINT('Ctrl Pts',(117.90964389367,1.53249139509446,340.714840390288));
#12613=CARTESIAN_POINT('Ctrl Pts',(117.905786768516,1.61125885188146,340.693718111887));
#12614=CARTESIAN_POINT('Ctrl Pts',(117.901929643361,1.68953310047218,340.670982193367));
#12615=CARTESIAN_POINT('Ctrl Pts',(117.898072518206,1.76724436844757,340.646660774714));
#12616=CARTESIAN_POINT('Ctrl Pts',(117.890648540768,1.9168186438438,340.599848276778));
#12617=CARTESIAN_POINT('Ctrl Pts',(117.88322456333,2.06475725202675,340.547017951053));
#12618=CARTESIAN_POINT('Ctrl Pts',(117.875800585892,2.21053929064311,340.488300885249));
#12619=CARTESIAN_POINT('Ctrl Pts',(117.868385369865,2.35614928451976,340.429653114417));
#12620=CARTESIAN_POINT('Ctrl Pts',(117.860970153837,2.49960743202581,340.365132570175));
#12621=CARTESIAN_POINT('Ctrl Pts',(117.85355493781,2.64040692058352,340.294920382426));
#12622=CARTESIAN_POINT('Ctrl Pts',(117.846146856665,2.78107093258252,340.224775752492));
#12623=CARTESIAN_POINT('Ctrl Pts',(117.838738775521,2.91908104667356,340.148950547119));
#12624=CARTESIAN_POINT('Ctrl Pts',(117.831330694377,3.05394951751189,340.067674309482));
#12625=CARTESIAN_POINT('Ctrl Pts',(117.823928127203,3.18871760328419,339.986458567234));
#12626=CARTESIAN_POINT('Ctrl Pts',(117.816525560029,3.32034838357892,339.89980006321));
#12627=CARTESIAN_POINT('Ctrl Pts',(117.809122992855,3.44837796508353,339.80797462269));
#12628=CARTESIAN_POINT('Ctrl Pts',(117.8017243231,3.57634013957339,339.716197527862));
#12629=CARTESIAN_POINT('Ctrl Pts',(117.794325653346,3.70070458879116,339.619259131281));
#12630=CARTESIAN_POINT('Ctrl Pts',(117.786926983591,3.82103581280916,339.517478929639));
#12631=CARTESIAN_POINT('Ctrl Pts',(117.779529534387,3.94134718591134,339.41571551857));
#12632=CARTESIAN_POINT('Ctrl Pts',(117.772132085183,4.05762636966001,339.309112128482));
#12633=CARTESIAN_POINT('Ctrl Pts',(117.764734635979,4.1694703360073,339.198029023203));
#12634=CARTESIAN_POINT('Ctrl Pts',(117.757337507515,4.28130945299508,339.086950734295));
#12635=CARTESIAN_POINT('Ctrl Pts',(117.749940379052,4.38871347014439,338.971393379392));
#12636=CARTESIAN_POINT('Ctrl Pts',(117.742543250588,4.49131588602363,338.851754428108));
#12637=CARTESIAN_POINT('Ctrl Pts',(117.735144983152,4.59393410011392,338.732097055412));
#12638=CARTESIAN_POINT('Ctrl Pts',(117.727746715715,4.69174899786508,338.608357118295));
#12639=CARTESIAN_POINT('Ctrl Pts',(117.720348448279,4.78443417554128,338.48096540954));
#12640=CARTESIAN_POINT('Ctrl Pts',(117.712947581753,4.87715191449527,338.353528946737));
#12641=CARTESIAN_POINT('Ctrl Pts',(117.705546715227,4.96473612591647,338.22243845963));
#12642=CARTESIAN_POINT('Ctrl Pts',(117.698145848701,5.04690365202663,338.088153831929));
#12643=CARTESIAN_POINT('Ctrl Pts',(117.690736855316,5.12916140593576,337.95372174687));
#12644=CARTESIAN_POINT('Ctrl Pts',(117.683327861932,5.20599040107577,337.816088835141));
#12645=CARTESIAN_POINT('Ctrl Pts',(117.675918868547,5.27715303870011,337.675740340287));
#12646=CARTESIAN_POINT('Ctrl Pts',(117.668505310967,5.34835951496366,337.535305385919));
#12647=CARTESIAN_POINT('Ctrl Pts',(117.661091753386,5.41389252310431,337.392151853515));
#12648=CARTESIAN_POINT('Ctrl Pts',(117.653678195806,5.47356278320716,337.246784595993));
#12649=CARTESIAN_POINT('Ctrl Pts',(117.64625408367,5.53331799484952,337.101210381566));
#12650=CARTESIAN_POINT('Ctrl Pts',(117.638829971533,5.58719366095912,336.953416497253));
#12651=CARTESIAN_POINT('Ctrl Pts',(117.631405859396,5.63505023319088,336.803923344246));
#12652=CARTESIAN_POINT('Ctrl Pts',(117.627548734242,5.65991364920208,336.726255632567));
#12653=CARTESIAN_POINT('Ctrl Pts',(117.623691609087,5.68315321755644,336.648129436923));
#12654=CARTESIAN_POINT('Ctrl Pts',(117.619834483932,5.70475484390881,336.569618658592));
#12655=CARTESIAN_POINT('Ctrl Pts',(117.612410506494,5.74633243868109,336.41850553065));
#12656=CARTESIAN_POINT('Ctrl Pts',(117.604986529056,5.78196436029644,336.265511278244));
#12657=CARTESIAN_POINT('Ctrl Pts',(117.597562551618,5.81147895305511,336.111144878356));
#12658=CARTESIAN_POINT('Ctrl Pts',(117.590147335591,5.84095871415357,335.956960654047));
#12659=CARTESIAN_POINT('Ctrl Pts',(117.582732119563,5.864335447257,335.801407868586));
#12660=CARTESIAN_POINT('Ctrl Pts',(117.575316903535,5.88148720299975,335.645010731267));
#12661=CARTESIAN_POINT('Ctrl Pts',(117.567908822391,5.89862245540953,335.488764078487));
#12662=CARTESIAN_POINT('Ctrl Pts',(117.560500741247,5.90954461430555,335.331675059754));
#12663=CARTESIAN_POINT('Ctrl Pts',(117.553092660103,5.91418276044594,335.174278049519));
#12664=CARTESIAN_POINT('Ctrl Pts',(117.545690092929,5.91881745432944,335.016998192753));
#12665=CARTESIAN_POINT('Ctrl Pts',(117.538287525755,5.91717743770786,334.859411172393));
#12666=CARTESIAN_POINT('Ctrl Pts',(117.530884958581,5.90924361865239,334.702056351106));
#12667=CARTESIAN_POINT('Ctrl Pts',(117.523486288826,5.90131397671794,334.544784376445));
#12668=CARTESIAN_POINT('Ctrl Pts',(117.516087619072,5.88709715044508,334.387744729184));
#12669=CARTESIAN_POINT('Ctrl Pts',(117.508688949317,5.8666261374193,334.231476528498));
#12670=CARTESIAN_POINT('Ctrl Pts',(117.501291500113,5.84615850147507,334.075234107214));
#12671=CARTESIAN_POINT('Ctrl Pts',(117.493894050909,5.81943877489074,333.919763249614));
#12672=CARTESIAN_POINT('Ctrl Pts',(117.486496601705,5.78655180960394,333.765597830013));
#12673=CARTESIAN_POINT('Ctrl Pts',(117.479099473241,5.75366627023858,333.611439094755));
#12674=CARTESIAN_POINT('Ctrl Pts',(117.471702344778,5.71461410171396,333.458586049953));
#12675=CARTESIAN_POINT('Ctrl Pts',(117.464305216314,5.66953120975157,333.307561988091));
#12676=CARTESIAN_POINT('Ctrl Pts',(117.456906948878,5.62444137614927,333.156514672295));
#12677=CARTESIAN_POINT('Ctrl Pts',(117.449508681441,5.57331907694302,333.007297257817));
#12678=CARTESIAN_POINT('Ctrl Pts',(117.442110414005,5.51634993918263,332.860417351215));
#12679=CARTESIAN_POINT('Ctrl Pts',(117.434709547479,5.45936078756483,332.713485844158));
#12680=CARTESIAN_POINT('Ctrl Pts',(117.427308680953,5.39652084264469,332.568893827702));
#12681=CARTESIAN_POINT('Ctrl Pts',(117.419907814427,5.32806359752402,332.427128284729));
#12682=CARTESIAN_POINT('Ctrl Pts',(117.412498821042,5.2595311798037,332.285207069638));
#12683=CARTESIAN_POINT('Ctrl Pts',(117.405089827658,5.18536930577916,332.146118862639));
#12684=CARTESIAN_POINT('Ctrl Pts',(117.397680834273,5.10585744878188,332.010326058712));
#12685=CARTESIAN_POINT('Ctrl Pts',(117.390267276693,5.02629660973784,331.874449601733));
#12686=CARTESIAN_POINT('Ctrl Pts',(117.382853719112,4.94137942128065,331.74187290657));
#12687=CARTESIAN_POINT('Ctrl Pts',(117.375440161532,4.85142799477547,331.613028347623));
#12688=CARTESIAN_POINT('Ctrl Pts',(117.368016049395,4.76134850594714,331.484000354858));
#12689=CARTESIAN_POINT('Ctrl Pts',(117.360591937259,4.66622068990136,331.358715406627));
#12690=CARTESIAN_POINT('Ctrl Pts',(117.353167825122,4.56640664548534,331.237572471054));
#12691=CARTESIAN_POINT('Ctrl Pts',(117.349310699967,4.51454923083325,331.174633838732));
#12692=CARTESIAN_POINT('Ctrl Pts',(117.345453574813,4.46142751009049,331.112812622566));
#12693=CARTESIAN_POINT('Ctrl Pts',(117.341596449658,4.4070960011583,331.052160667014));
#12694=CARTESIAN_POINT('Ctrl Pts',(117.33417247222,4.30252177026849,330.935421196152));
#12695=CARTESIAN_POINT('Ctrl Pts',(117.326748494782,4.19314811677626,330.822663584307));
#12696=CARTESIAN_POINT('Ctrl Pts',(117.319324517344,4.07931015753743,330.714307617069));
#12697=CARTESIAN_POINT('Ctrl Pts',(117.311909301317,3.96560654421835,330.606079526176));
#12698=CARTESIAN_POINT('Ctrl Pts',(117.304494085289,3.84744937999032,330.502242994759));
#12699=CARTESIAN_POINT('Ctrl Pts',(117.297078869262,3.72521348983267,330.403184252369));
#12700=CARTESIAN_POINT('Ctrl Pts',(117.289670788117,3.60309521443302,330.304220823803));
#12701=CARTESIAN_POINT('Ctrl Pts',(117.282262706973,3.4769063141263,330.210026265571));
#12702=CARTESIAN_POINT('Ctrl Pts',(117.274854625829,3.34705777731504,330.120949395854));
#12703=CARTESIAN_POINT('Ctrl Pts',(117.267452058655,3.21730588914142,330.031938827679));
#12704=CARTESIAN_POINT('Ctrl Pts',(117.260049491481,3.08390009465115,329.948038573586));
#12705=CARTESIAN_POINT('Ctrl Pts',(117.252646924307,2.94728362368041,329.869556568474));
#12706=CARTESIAN_POINT('Ctrl Pts',(117.245248254553,2.81073908068388,329.791115883795));
#12707=CARTESIAN_POINT('Ctrl Pts',(117.237849584798,2.67098755055128,329.718087952245));
#12708=CARTESIAN_POINT('Ctrl Pts',(117.230450915043,2.52850024698414,329.65073677377));
#12709=CARTESIAN_POINT('Ctrl Pts',(117.223053465839,2.38603644939812,329.583396706147));
#12710=CARTESIAN_POINT('Ctrl Pts',(117.215656016635,2.24083811118513,329.521731692309));
#12711=CARTESIAN_POINT('Ctrl Pts',(117.208258567431,2.09340009689756,329.465959288476));
#12712=CARTESIAN_POINT('Ctrl Pts',(117.200861438968,1.94596847526519,329.410189302836));
#12713=CARTESIAN_POINT('Ctrl Pts',(117.193464310504,1.79629771971294,329.360311551241));
#12714=CARTESIAN_POINT('Ctrl Pts',(117.186067182041,1.64490142444076,329.316494931262));
#12715=CARTESIAN_POINT('Ctrl Pts',(117.178668914604,1.49348181791837,329.272671564617));
#12716=CARTESIAN_POINT('Ctrl Pts',(117.171270647168,1.34033650117289,329.234911291598));
#12717=CARTESIAN_POINT('Ctrl Pts',(117.163872379731,1.18599278483601,329.203332709494));
#12718=CARTESIAN_POINT('Ctrl Pts',(117.156471513205,1.03159484592813,329.171743033503));
#12719=CARTESIAN_POINT('Ctrl Pts',(117.149070646679,0.875998034604377,329.146339447025));
#12720=CARTESIAN_POINT('Ctrl Pts',(117.141669780154,0.719738221673399,329.127189135111));
#12721=CARTESIAN_POINT('Ctrl Pts',(117.134260786769,0.563306820529132,329.108017794323));
#12722=CARTESIAN_POINT('Ctrl Pts',(117.126851793384,0.406211334505276,329.095113486677));
#12723=CARTESIAN_POINT('Ctrl Pts',(117.119442799999,0.248991840460065,329.088491425543));
#12724=CARTESIAN_POINT('Ctrl Pts',(117.112029242419,0.0916754937840028,
329.08186528499));
#12725=CARTESIAN_POINT('Ctrl Pts',(117.104615684839,-0.0657646407985479,
329.08152910339));
#12726=CARTESIAN_POINT('Ctrl Pts',(117.097202127259,-0.222790657487817,
329.087445993022));
#12727=CARTESIAN_POINT('Ctrl Pts',(117.089778015122,-0.380040229459693,
329.093371306429));
#12728=CARTESIAN_POINT('Ctrl Pts',(117.082353902985,-0.536874134959452,
329.105567442068));
#12729=CARTESIAN_POINT('Ctrl Pts',(117.074929790849,-0.692760920715127,
329.123945807838));
#12730=CARTESIAN_POINT('Ctrl Pts',(117.071072665694,-0.773750382023262,
329.133494108781));
#12731=CARTESIAN_POINT('Ctrl Pts',(117.067215540539,-0.854484372817623,
329.144710289688));
#12732=CARTESIAN_POINT('Ctrl Pts',(117.063358415384,-0.934889793223836,
329.157576561304));
#12733=CARTESIAN_POINT('Ctrl Pts',(117.055934437946,-1.08964962160184,329.18234083686));
#12734=CARTESIAN_POINT('Ctrl Pts',(117.048510460508,-1.24365826274491,329.213295861666));
#12735=CARTESIAN_POINT('Ctrl Pts',(117.04108648307,-1.3963813590339,329.25038699888));
#12736=CARTESIAN_POINT('Ctrl Pts',(117.033671267043,-1.54892421909094,329.287434362972));
#12737=CARTESIAN_POINT('Ctrl Pts',(117.026256051015,-1.70018419503602,329.330603337855));
#12738=CARTESIAN_POINT('Ctrl Pts',(117.018840834987,-1.84963365889594,329.379787736181));
#12739=CARTESIAN_POINT('Ctrl Pts',(117.011432753843,-1.99893932323336,329.428924809526));
#12740=CARTESIAN_POINT('Ctrl Pts',(117.004024672699,-2.14643759147631,329.484065667575));
#12741=CARTESIAN_POINT('Ctrl Pts',(116.996616591555,-2.29161272556869,329.545053466943));
#12742=CARTESIAN_POINT('Ctrl Pts',(116.989214024381,-2.43667980315796,329.605995871978));
#12743=CARTESIAN_POINT('Ctrl Pts',(116.981811457207,-2.57942684698023,329.672776408968));
#12744=CARTESIAN_POINT('Ctrl Pts',(116.974408890033,-2.71935505091292,329.74518899773));
#12745=CARTESIAN_POINT('Ctrl Pts',(116.967010220278,-2.85920958325803,329.817563461581));
#12746=CARTESIAN_POINT('Ctrl Pts',(116.959611550524,-2.99624790077714,329.895563900634));
#12747=CARTESIAN_POINT('Ctrl Pts',(116.952212880769,-3.12999299951152,329.978936926755));
#12748=CARTESIAN_POINT('Ctrl Pts',(116.944815431565,-3.26371603445751,330.062296198914));
#12749=CARTESIAN_POINT('Ctrl Pts',(116.937417982361,-3.39414661244574,330.151026101863));
#12750=CARTESIAN_POINT('Ctrl Pts',(116.930020533157,-3.52083398620457,330.244828225596));
#12751=CARTESIAN_POINT('Ctrl Pts',(116.922623404693,-3.64751586702006,330.338626282233));
#12752=CARTESIAN_POINT('Ctrl Pts',(116.91522627623,-3.77045456636731,330.43749590029));
#12753=CARTESIAN_POINT('Ctrl Pts',(116.907829147766,-3.8892301193846,330.541096587616));
#12754=CARTESIAN_POINT('Ctrl Pts',(116.90043088033,-4.0080239608718,330.644713226861));
#12755=CARTESIAN_POINT('Ctrl Pts',(116.893032612893,-4.12265309840092,330.75306214051));
#12756=CARTESIAN_POINT('Ctrl Pts',(116.885634345456,-4.23273244294201,330.865764081603));
#12757=CARTESIAN_POINT('Ctrl Pts',(116.87823347893,-4.34285045951512,330.978505616073));
#12758=CARTESIAN_POINT('Ctrl Pts',(116.870832612405,-4.44841524009691,331.095602955928));
#12759=CARTESIAN_POINT('Ctrl Pts',(116.863431745879,-4.54908029690349,331.216641833658));
#12760=CARTESIAN_POINT('Ctrl Pts',(116.856022752494,-4.64985589356604,331.337813623648));
#12761=CARTESIAN_POINT('Ctrl Pts',(116.848613759109,-4.74572078279138,331.462935308015));
#12762=CARTESIAN_POINT('Ctrl Pts',(116.841204765724,-4.83636990475578,331.591560957436));
#12763=CARTESIAN_POINT('Ctrl Pts',(116.833791208144,-4.92707486970636,331.720265844694));
#12764=CARTESIAN_POINT('Ctrl Pts',(116.826377650564,-5.01255746272204,331.852478685551));
#12765=CARTESIAN_POINT('Ctrl Pts',(116.818964092983,-5.09255761178139,331.987727181481));
#12766=CARTESIAN_POINT('Ctrl Pts',(116.811539980847,-5.17267165569857,332.123168228405));
#12767=CARTESIAN_POINT('Ctrl Pts',(116.80411586871,-5.24728749044024,332.261653234254));
#12768=CARTESIAN_POINT('Ctrl Pts',(116.796691756573,-5.31619201513312,332.402687346365));
#12769=CARTESIAN_POINT('Ctrl Pts',(116.792834631419,-5.35199068984995,332.475960245727));
#12770=CARTESIAN_POINT('Ctrl Pts',(116.788977506264,-5.38624855896848,332.549920900035));
#12771=CARTESIAN_POINT('Ctrl Pts',(116.78512038111,-5.41894102331701,332.624498211259));
#12772=CARTESIAN_POINT('Ctrl Pts',(116.776934824929,-5.488320676014,332.782765507863));
#12773=CARTESIAN_POINT('Ctrl Pts',(116.768749268748,-5.55082719148128,332.944220960742));
#12774=CARTESIAN_POINT('Ctrl Pts',(116.760563712567,-5.60618584572961,333.108278343508));
#12775=CARTESIAN_POINT('Ctrl Pts',(116.752409291884,-5.6613339315994,333.271711699235));
#12776=CARTESIAN_POINT('Ctrl Pts',(116.744254871202,-5.70938830934361,333.437727012654));
#12777=CARTESIAN_POINT('Ctrl Pts',(116.736100450519,-5.75012310339411,333.605720667042));
#12778=CARTESIAN_POINT('Ctrl Pts',(116.727965705022,-5.79075961153875,333.773308982239));
#12779=CARTESIAN_POINT('Ctrl Pts',(116.719830959525,-5.82411169567996,333.942865884475));
#12780=CARTESIAN_POINT('Ctrl Pts',(116.711696214028,-5.85000251100064,334.113771370477));
#12781=CARTESIAN_POINT('Ctrl Pts',(116.703593916848,-5.87579005161965,334.28399513932));
#12782=CARTESIAN_POINT('Ctrl Pts',(116.695491619669,-5.89417563440154,334.455556524049));
#12783=CARTESIAN_POINT('Ctrl Pts',(116.68738932249,-5.90503317782377,334.62782567082));
#12784=CARTESIAN_POINT('Ctrl Pts',(116.681610235614,-5.91277748605137,334.750699263752));
#12785=CARTESIAN_POINT('Ctrl Pts',(116.675831148737,-5.91669293342916,334.873932560887));
#12786=CARTESIAN_POINT('Ctrl Pts',(116.67005206186,-5.91674938057594,334.997292611182));
#12787=CARTESIAN_POINT('',(114.920051985967,-5.91445891360904,335.005133702733));
#12788=CARTESIAN_POINT('Ctrl Pts',(116.670052004703,-5.90815805324423,334.997297760704));
#12789=CARTESIAN_POINT('Ctrl Pts',(116.615662118748,-5.90339216544283,336.156617696109));
#12790=CARTESIAN_POINT('Ctrl Pts',(116.468526221367,-5.01269847614412,339.29957741469));
#12791=CARTESIAN_POINT('Ctrl Pts',(116.228644312563,0.0981603043517565,
341.995926491601));
#12792=CARTESIAN_POINT('Ctrl Pts',(115.950406278288,5.93614401145467,338.703352156694));
#12793=CARTESIAN_POINT('Ctrl Pts',(115.672168244014,6.32661597658701,332.012266208978));
#12794=CARTESIAN_POINT('Ctrl Pts',(115.39393020974,0.911245840702667,328.062979462403));
#12795=CARTESIAN_POINT('Ctrl Pts',(115.143224796637,-4.72174289882804,330.240551757169));
#12796=CARTESIAN_POINT('Ctrl Pts',(114.985265394958,-5.9015978468786,333.617997724062));
#12797=CARTESIAN_POINT('Ctrl Pts',(114.920052004703,-5.91304802076869,335.005132079402));
#12798=CARTESIAN_POINT('',(113.170052004703,-5.92205629387471,335.000268163494));
#12799=CARTESIAN_POINT('Ctrl Pts',(114.920051955571,-5.91674777057043,335.005136336223));
#12800=CARTESIAN_POINT('Ctrl Pts',(114.911108166502,-5.91658252040811,335.19549449953));
#12801=CARTESIAN_POINT('Ctrl Pts',(114.902164377432,-5.90722704884812,335.385450638901));
#12802=CARTESIAN_POINT('Ctrl Pts',(114.893220588363,-5.88881999184248,335.574220921054));
#12803=CARTESIAN_POINT('Ctrl Pts',(114.883926180501,-5.86969133238817,335.770391468106));
#12804=CARTESIAN_POINT('Ctrl Pts',(114.874631772639,-5.8407873268764,335.965281261497));
#12805=CARTESIAN_POINT('Ctrl Pts',(114.865337364778,-5.80231725333009,336.15803499697));
#12806=CARTESIAN_POINT('Ctrl Pts',(114.856042956916,-5.76384717978377,336.350788732443));
#12807=CARTESIAN_POINT('Ctrl Pts',(114.846748549055,-5.71581115839886,336.541406475282));
#12808=CARTESIAN_POINT('Ctrl Pts',(114.837454141193,-5.65847091140766,336.729056825918));
#12809=CARTESIAN_POINT('Ctrl Pts',(114.830030163755,-5.61266996246214,336.87894393977));
#12810=CARTESIAN_POINT('Ctrl Pts',(114.822606186317,-5.56084027295747,337.027236078446));
#12811=CARTESIAN_POINT('Ctrl Pts',(114.815182208879,-5.50310940854717,337.173411465889));
#12812=CARTESIAN_POINT('Ctrl Pts',(114.807766992851,-5.44544667524294,337.319414344382));
#12813=CARTESIAN_POINT('Ctrl Pts',(114.800351776824,-5.38189676529112,337.463305100375));
#12814=CARTESIAN_POINT('Ctrl Pts',(114.792936560796,-5.31263738058319,337.604575709195));
#12815=CARTESIAN_POINT('Ctrl Pts',(114.785528479652,-5.24344463690651,337.745710388147));
#12816=CARTESIAN_POINT('Ctrl Pts',(114.778120398508,-5.1685535184537,337.884229606084));
#12817=CARTESIAN_POINT('Ctrl Pts',(114.770712317364,-5.08819026809218,338.019644078065));
#12818=CARTESIAN_POINT('Ctrl Pts',(114.76330975019,-5.00788683356546,338.154957758582));
#12819=CARTESIAN_POINT('Ctrl Pts',(114.755907183016,-4.92211956673602,338.287170974945));
#12820=CARTESIAN_POINT('Ctrl Pts',(114.748504615842,-4.83116115265796,338.415817981033));
#12821=CARTESIAN_POINT('Ctrl Pts',(114.741105946087,-4.74025062778728,338.544397255035));
#12822=CARTESIAN_POINT('Ctrl Pts',(114.733707276332,-4.64415461374849,338.669413754133));
#12823=CARTESIAN_POINT('Ctrl Pts',(114.726308606577,-4.5431896578316,338.79042982991));
#12824=CARTESIAN_POINT('Ctrl Pts',(114.718911157373,-4.44224135799756,338.911425941792));
#12825=CARTESIAN_POINT('Ctrl Pts',(114.71151370817,-4.33642594928277,339.02842265384));
#12826=CARTESIAN_POINT('Ctrl Pts',(114.704116258965,-4.22610096455406,339.141014513364));
#12827=CARTESIAN_POINT('Ctrl Pts',(114.696719130502,-4.11578076332436,339.253601491102));
#12828=CARTESIAN_POINT('Ctrl Pts',(114.689322002038,-4.00095163605661,339.36178372949));
#12829=CARTESIAN_POINT('Ctrl Pts',(114.681924873575,-3.88200856731397,339.465192050271));
#12830=CARTESIAN_POINT('Ctrl Pts',(114.674526606138,-3.76304718430788,339.568616293351));
#12831=CARTESIAN_POINT('Ctrl Pts',(114.667128338702,-3.6399708802243,339.667264910334));
#12832=CARTESIAN_POINT('Ctrl Pts',(114.659730071265,-3.51320823292414,339.760808594621));
#12833=CARTESIAN_POINT('Ctrl Pts',(114.652329204739,-3.38640105257265,339.854385141787));
#12834=CARTESIAN_POINT('Ctrl Pts',(114.644928338213,-3.25590525066864,339.942852964104));
#12835=CARTESIAN_POINT('Ctrl Pts',(114.637527471688,-3.12217878749545,340.025925803413));
#12836=CARTESIAN_POINT('Ctrl Pts',(114.630118478303,-2.98830547988117,340.109089864642));
#12837=CARTESIAN_POINT('Ctrl Pts',(114.622709484918,-2.8511947435109,340.186846914849));
#12838=CARTESIAN_POINT('Ctrl Pts',(114.615300491533,-2.7113302057046,340.258956082545));
#12839=CARTESIAN_POINT('Ctrl Pts',(114.607886933953,-2.57137950651857,340.331109671975));
#12840=CARTESIAN_POINT('Ctrl Pts',(114.600473376373,-2.42867196301874,340.397608288682));
#12841=CARTESIAN_POINT('Ctrl Pts',(114.593059818792,-2.28371113788016,340.458259246428));
#12842=CARTESIAN_POINT('Ctrl Pts',(114.585635706656,-2.13854393446848,340.518996551917));
#12843=CARTESIAN_POINT('Ctrl Pts',(114.578211594519,-1.99111739130797,340.573869441495));
#12844=CARTESIAN_POINT('Ctrl Pts',(114.570787482382,-1.84195095496589,340.622734854321));
#12845=CARTESIAN_POINT('Ctrl Pts',(114.566930357228,-1.76445298574589,340.648122403639));
#12846=CARTESIAN_POINT('Ctrl Pts',(114.563073232073,-1.68648557277676,340.671889239741));
#12847=CARTESIAN_POINT('Ctrl Pts',(114.559216106918,-1.60812252043137,340.694020769349));
#12848=CARTESIAN_POINT('Ctrl Pts',(114.55179212948,-1.45729372715926,340.736618292087));
#12849=CARTESIAN_POINT('Ctrl Pts',(114.544368152042,-1.30454368509424,340.773282985683));
#12850=CARTESIAN_POINT('Ctrl Pts',(114.536944174604,-1.15038019994917,340.803839759854));
#12851=CARTESIAN_POINT('Ctrl Pts',(114.529528958576,-0.996398650911766,
340.834360472434));
#12852=CARTESIAN_POINT('Ctrl Pts',(114.522113742549,-0.841007341654273,
340.858787541895));
#12853=CARTESIAN_POINT('Ctrl Pts',(114.514698526521,-0.684729645653049,
340.876995480249));
#12854=CARTESIAN_POINT('Ctrl Pts',(114.507290445377,-0.528602319264051,
340.895185899015));
#12855=CARTESIAN_POINT('Ctrl Pts',(114.499882364233,-0.371590672276281,
340.907169056833));
#12856=CARTESIAN_POINT('Ctrl Pts',(114.492474283089,-0.214228587833211,
340.912870425999));
#12857=CARTESIAN_POINT('Ctrl Pts',(114.485071715915,-0.0569836308636502,
340.918567551532));
#12858=CARTESIAN_POINT('Ctrl Pts',(114.477669148741,0.100610872827737,340.917992184858));
#12859=CARTESIAN_POINT('Ctrl Pts',(114.470266581567,0.258015701860771,340.911121590705));
#12860=CARTESIAN_POINT('Ctrl Pts',(114.462867911812,0.415337657939364,340.904254613889));
#12861=CARTESIAN_POINT('Ctrl Pts',(114.455469242057,0.572469766325245,340.891099026673));
#12862=CARTESIAN_POINT('Ctrl Pts',(114.448070572303,0.728872697225493,340.871684183753));
#12863=CARTESIAN_POINT('Ctrl Pts',(114.440673123099,0.885249826498768,340.85227254368));
#12864=CARTESIAN_POINT('Ctrl Pts',(114.433275673895,1.04089764701791,340.826603743178));
#12865=CARTESIAN_POINT('Ctrl Pts',(114.425878224691,1.19528172341699,340.794759025548));
#12866=CARTESIAN_POINT('Ctrl Pts',(114.418481096227,1.34965910599172,340.762915688648));
#12867=CARTESIAN_POINT('Ctrl Pts',(114.411083967764,1.50277248787793,340.724897042444));
#12868=CARTESIAN_POINT('Ctrl Pts',(114.4036868393,1.65409767039088,340.680835454342));
#12869=CARTESIAN_POINT('Ctrl Pts',(114.396288571864,1.8054461532044,340.636767081855));
#12870=CARTESIAN_POINT('Ctrl Pts',(114.388890304427,1.95500553005805,340.586654019139));
#12871=CARTESIAN_POINT('Ctrl Pts',(114.381492036991,2.10226695193475,340.530678459764));
#12872=CARTESIAN_POINT('Ctrl Pts',(114.374091170465,2.2495801082977,340.474683235587));
#12873=CARTESIAN_POINT('Ctrl Pts',(114.366690303939,2.39459335372001,340.412821546699));
#12874=CARTESIAN_POINT('Ctrl Pts',(114.359289437413,2.53681813902212,340.345323590956));
#12875=CARTESIAN_POINT('Ctrl Pts',(114.351880444029,2.67919910073561,340.277751516005));
#12876=CARTESIAN_POINT('Ctrl Pts',(114.344471450644,2.81878514999127,340.204530974227));
#12877=CARTESIAN_POINT('Ctrl Pts',(114.337062457259,2.9551120143209,340.12593830877));
#12878=CARTESIAN_POINT('Ctrl Pts',(114.329648899679,3.09152286070137,340.04729722752));
#12879=CARTESIAN_POINT('Ctrl Pts',(114.322235342099,3.22467020652081,339.963277626849));
#12880=CARTESIAN_POINT('Ctrl Pts',(114.314821784519,3.35411951115436,339.874198689774));
#12881=CARTESIAN_POINT('Ctrl Pts',(114.307397672382,3.48375311057188,339.784992932524));
#12882=CARTESIAN_POINT('Ctrl Pts',(114.299973560245,3.60967785591732,339.690713676329));
#12883=CARTESIAN_POINT('Ctrl Pts',(114.292549448109,3.73149234193394,339.59172031646));
#12884=CARTESIAN_POINT('Ctrl Pts',(114.288692322954,3.79477987175087,339.54028928047));
#12885=CARTESIAN_POINT('Ctrl Pts',(114.284835197799,3.85695855219829,339.487586418299));
#12886=CARTESIAN_POINT('Ctrl Pts',(114.280978072645,3.91797617169529,339.433665896358));
#12887=CARTESIAN_POINT('Ctrl Pts',(114.273554095207,4.03541945193731,339.329882710103));
#12888=CARTESIAN_POINT('Ctrl Pts',(114.266130117769,4.14891338754633,339.221273310476));
#12889=CARTESIAN_POINT('Ctrl Pts',(114.258706140331,4.25803593855763,339.108169970735));
#12890=CARTESIAN_POINT('Ctrl Pts',(114.251290924303,4.36702970854041,338.995200109953));
#12891=CARTESIAN_POINT('Ctrl Pts',(114.243875708276,4.47166210616983,338.87774713178));
#12892=CARTESIAN_POINT('Ctrl Pts',(114.236460492248,4.5715443784989,338.756183243389));
#12893=CARTESIAN_POINT('Ctrl Pts',(114.229052411104,4.67133054460841,338.634736323159));
#12894=CARTESIAN_POINT('Ctrl Pts',(114.22164432996,4.76637544917839,338.509186653799));
#12895=CARTESIAN_POINT('Ctrl Pts',(114.214236248816,4.85632750546997,338.379942857818));
#12896=CARTESIAN_POINT('Ctrl Pts',(114.206833681642,4.9462126088032,338.250795260355));
#12897=CARTESIAN_POINT('Ctrl Pts',(114.199431114468,5.03101219941007,338.117959316148));
#12898=CARTESIAN_POINT('Ctrl Pts',(114.192028547294,5.11041535508601,337.981876164599));
#12899=CARTESIAN_POINT('Ctrl Pts',(114.184629877539,5.18977670534751,337.845864660234));
#12900=CARTESIAN_POINT('Ctrl Pts',(114.177231207785,5.26374709148096,337.706609674915));
#12901=CARTESIAN_POINT('Ctrl Pts',(114.16983253803,5.332059336181,337.564580628084));
#12902=CARTESIAN_POINT('Ctrl Pts',(114.162435088826,5.40036031148194,337.422575011636));
#12903=CARTESIAN_POINT('Ctrl Pts',(114.155037639622,5.46300483627296,337.277796577933));
#12904=CARTESIAN_POINT('Ctrl Pts',(114.147640190418,5.51977201613607,337.13073871049));
#12905=CARTESIAN_POINT('Ctrl Pts',(114.140243061954,5.5765367346732,336.98368721922));
#12906=CARTESIAN_POINT('Ctrl Pts',(114.132845933491,5.62742448057049,336.834356838891));
#12907=CARTESIAN_POINT('Ctrl Pts',(114.125448805028,5.67226289041743,336.683260010959));
#12908=CARTESIAN_POINT('Ctrl Pts',(114.118050537591,5.71710820426018,336.532139917888));
#12909=CARTESIAN_POINT('Ctrl Pts',(114.110652270154,5.75590222123792,336.37925319346));
#12910=CARTESIAN_POINT('Ctrl Pts',(114.103254002718,5.78852278440978,336.225126335065));
#12911=CARTESIAN_POINT('Ctrl Pts',(114.095853136192,5.82115480752854,336.070945330283));
#12912=CARTESIAN_POINT('Ctrl Pts',(114.088452269666,5.84760898153712,335.915523689005));
#12913=CARTESIAN_POINT('Ctrl Pts',(114.081051403141,5.86781450273083,335.759396815928));
#12914=CARTESIAN_POINT('Ctrl Pts',(114.073642409756,5.88804221151854,335.603098500618));
#12915=CARTESIAN_POINT('Ctrl Pts',(114.066233416371,5.90200751654431,335.446093777312));
#12916=CARTESIAN_POINT('Ctrl Pts',(114.058824422986,5.9096915561831,335.288922607766));
#12917=CARTESIAN_POINT('Ctrl Pts',(114.051410865406,5.91738032945537,335.131654615358));
#12918=CARTESIAN_POINT('Ctrl Pts',(114.043997307826,5.91878012358746,334.974220344718));
#12919=CARTESIAN_POINT('Ctrl Pts',(114.036583750246,5.91392419152231,334.817157938572));
#12920=CARTESIAN_POINT('Ctrl Pts',(114.029159638109,5.90906134614886,334.659871925337));
#12921=CARTESIAN_POINT('Ctrl Pts',(114.021735525972,5.89792501352182,334.50295920522));
#12922=CARTESIAN_POINT('Ctrl Pts',(114.014311413836,5.88060019337428,334.346951817868));
#12923=CARTESIAN_POINT('Ctrl Pts',(114.010454288681,5.87159925179876,334.265899699176));
#12924=CARTESIAN_POINT('Ctrl Pts',(114.006597163526,5.86092874243482,334.185091777452));
#12925=CARTESIAN_POINT('Ctrl Pts',(114.002740038371,5.84860596029069,334.10460127108));
#12926=CARTESIAN_POINT('Ctrl Pts',(113.995316060933,5.82488776268465,333.949677674021));
#12927=CARTESIAN_POINT('Ctrl Pts',(113.987892083495,5.79497388229717,333.795463424136));
#12928=CARTESIAN_POINT('Ctrl Pts',(113.980468106057,5.75891534475801,333.642493235961));
#12929=CARTESIAN_POINT('Ctrl Pts',(113.97305289003,5.72289936171842,333.489703575624));
#12930=CARTESIAN_POINT('Ctrl Pts',(113.965637674002,5.68075324078695,333.338155414284));
#12931=CARTESIAN_POINT('Ctrl Pts',(113.958222457975,5.63257960238745,333.188377085244));
#12932=CARTESIAN_POINT('Ctrl Pts',(113.95081437683,5.58445231642026,333.038742872159));
#12933=CARTESIAN_POINT('Ctrl Pts',(113.943406295686,5.53030917250915,332.890875454082));
#12934=CARTESIAN_POINT('Ctrl Pts',(113.935998214542,5.4703035262807,332.745291616891));
#12935=CARTESIAN_POINT('Ctrl Pts',(113.928595647368,5.41034254335067,332.599816140409));
#12936=CARTESIAN_POINT('Ctrl Pts',(113.921193080194,5.34452788821302,332.456621204012));
#12937=CARTESIAN_POINT('Ctrl Pts',(113.91379051302,5.27306226655672,332.316206994659));
#12938=CARTESIAN_POINT('Ctrl Pts',(113.906391843265,5.20163427123788,332.175866712774));
#12939=CARTESIAN_POINT('Ctrl Pts',(113.898993173511,5.12456140356545,332.03830457398));
#12940=CARTESIAN_POINT('Ctrl Pts',(113.891594503756,5.04209382339125,331.903999283169));
#12941=CARTESIAN_POINT('Ctrl Pts',(113.884197054552,4.95963984780696,331.76971614856));
#12942=CARTESIAN_POINT('Ctrl Pts',(113.876799605348,4.87179312110084,331.63868911334));
#12943=CARTESIAN_POINT('Ctrl Pts',(113.869402156144,4.77884900134984,331.511370930466));
#12944=CARTESIAN_POINT('Ctrl Pts',(113.862005027681,4.68590891149383,331.384058267887));
#12945=CARTESIAN_POINT('Ctrl Pts',(113.854607899217,4.58787208809426,331.260454439348));
#12946=CARTESIAN_POINT('Ctrl Pts',(113.847210770754,4.4850761783726,331.140981700394));
#12947=CARTESIAN_POINT('Ctrl Pts',(113.839812503317,4.38226444064697,331.021490565621));
#12948=CARTESIAN_POINT('Ctrl Pts',(113.83241423588,4.27469240096722,330.906132069884));
#12949=CARTESIAN_POINT('Ctrl Pts',(113.825015968444,4.16273669609027,330.795293855509));
#12950=CARTESIAN_POINT('Ctrl Pts',(113.817615101918,4.05074165999677,330.684416702503));
#12951=CARTESIAN_POINT('Ctrl Pts',(113.810214235392,3.93436015756705,330.578063255017));
#12952=CARTESIAN_POINT('Ctrl Pts',(113.802813368867,3.81400410608604,330.476582791599));
#12953=CARTESIAN_POINT('Ctrl Pts',(113.795404375482,3.69351589215392,330.37499089293));
#12954=CARTESIAN_POINT('Ctrl Pts',(113.787995382097,3.56904469865514,330.278282905287));
#12955=CARTESIAN_POINT('Ctrl Pts',(113.780586388712,3.44103438384275,330.186766894102));
#12956=CARTESIAN_POINT('Ctrl Pts',(113.773172831132,3.31294521026089,330.095194505897));
#12957=CARTESIAN_POINT('Ctrl Pts',(113.765759273552,3.18131288229146,330.008820671728));
#12958=CARTESIAN_POINT('Ctrl Pts',(113.758345715972,3.04660793071028,329.927908648394));
#12959=CARTESIAN_POINT('Ctrl Pts',(113.750921603835,2.91171120196967,329.846881431982));
#12960=CARTESIAN_POINT('Ctrl Pts',(113.743497491698,2.77373343945004,329.771331735166));
#12961=CARTESIAN_POINT('Ctrl Pts',(113.736073379561,2.63316804487387,329.701475997039));
#12962=CARTESIAN_POINT('Ctrl Pts',(113.732216254407,2.5601386631356,329.665183128643));
#12963=CARTESIAN_POINT('Ctrl Pts',(113.728359129252,2.48641113290674,329.630426384411));
#12964=CARTESIAN_POINT('Ctrl Pts',(113.724502004097,2.41205638441086,329.597230843269));
#12965=CARTESIAN_POINT('Ctrl Pts',(113.717078026659,2.26894254881944,329.533337933759));
#12966=CARTESIAN_POINT('Ctrl Pts',(113.709654049221,2.12307237893853,329.475038974537));
#12967=CARTESIAN_POINT('Ctrl Pts',(113.702230071783,1.97492314052506,329.422580421779));
#12968=CARTESIAN_POINT('Ctrl Pts',(113.694814855756,1.82694874050307,329.370183778007));
#12969=CARTESIAN_POINT('Ctrl Pts',(113.687399639728,1.67670097411336,329.323613944313));
#12970=CARTESIAN_POINT('Ctrl Pts',(113.6799844237,1.52467966190233,329.283070536461));
#12971=CARTESIAN_POINT('Ctrl Pts',(113.672576342556,1.37280462383236,329.242566139271));
#12972=CARTESIAN_POINT('Ctrl Pts',(113.665168261412,1.21915979545529,329.208076719528));
#12973=CARTESIAN_POINT('Ctrl Pts',(113.657760180268,1.06426274256818,329.179752979703));
#12974=CARTESIAN_POINT('Ctrl Pts',(113.650357613094,0.909480982386633,329.151450321754));
#12975=CARTESIAN_POINT('Ctrl Pts',(113.64295504592,0.753449219101078,329.129304272746));
#12976=CARTESIAN_POINT('Ctrl Pts',(113.635552478746,0.596697766275196,329.113415053002));
#12977=CARTESIAN_POINT('Ctrl Pts',(113.628153808991,0.440028842404039,329.097534198863));
#12978=CARTESIAN_POINT('Ctrl Pts',(113.620755139236,0.282641353994469,329.087903650952));
#12979=CARTESIAN_POINT('Ctrl Pts',(113.613356469482,0.125073230051813,329.084572099195));
#12980=CARTESIAN_POINT('Ctrl Pts',(113.605959020278,-0.0324689000430316,
329.081241097041));
#12981=CARTESIAN_POINT('Ctrl Pts',(113.598561571074,-0.190191233763988,
329.084207036568));
#12982=CARTESIAN_POINT('Ctrl Pts',(113.59116412187,-0.347553206286898,329.093466555474));
#12983=CARTESIAN_POINT('Ctrl Pts',(113.583766993406,-0.504908355869133,
329.102725672904));
#12984=CARTESIAN_POINT('Ctrl Pts',(113.576369864943,-0.661902802753377,
329.118277805216));
#12985=CARTESIAN_POINT('Ctrl Pts',(113.568972736479,-0.817998742957661,
329.140067524363));
#12986=CARTESIAN_POINT('Ctrl Pts',(113.561574469043,-0.974118718040169,
329.161860598584));
#12987=CARTESIAN_POINT('Ctrl Pts',(113.554176201606,-1.12933954132454,329.189893120387));
#12988=CARTESIAN_POINT('Ctrl Pts',(113.546777934169,-1.28313141634874,329.224058143395));
#12989=CARTESIAN_POINT('Ctrl Pts',(113.539377067643,-1.43697732007584,329.258235168935));
#12990=CARTESIAN_POINT('Ctrl Pts',(113.531976201118,-1.58939291195257,329.298548904225));
#12991=CARTESIAN_POINT('Ctrl Pts',(113.524575334592,-1.73986156411689,329.344841973896));
#12992=CARTESIAN_POINT('Ctrl Pts',(113.517166341207,-1.89049544524665,329.391185877784));
#12993=CARTESIAN_POINT('Ctrl Pts',(113.509757347822,-2.03917776018813,329.443522118657));
#12994=CARTESIAN_POINT('Ctrl Pts',(113.502348354438,-2.18540925297769,329.501644158523));
#12995=CARTESIAN_POINT('Ctrl Pts',(113.494934796857,-2.33173082941097,329.559802003571));
#12996=CARTESIAN_POINT('Ctrl Pts',(113.487521239277,-2.4755982349946,329.623752598616));
#12997=CARTESIAN_POINT('Ctrl Pts',(113.480107681697,-2.61653546026782,329.693242727648));
#12998=CARTESIAN_POINT('Ctrl Pts',(113.47268356956,-2.75767333548291,329.762831788601));
#12999=CARTESIAN_POINT('Ctrl Pts',(113.465259457423,-2.89587237177943,329.837975956743));
#13000=CARTESIAN_POINT('Ctrl Pts',(113.457835345287,-3.03068355292361,329.918377447651));
#13001=CARTESIAN_POINT('Ctrl Pts',(113.453978220132,-3.10072338911183,329.960149259194));
#13002=CARTESIAN_POINT('Ctrl Pts',(113.450121094978,-3.16984927392779,330.003339443623));
#13003=CARTESIAN_POINT('Ctrl Pts',(113.446263969823,-3.23800173355183,330.047901925848));
#13004=CARTESIAN_POINT('Ctrl Pts',(113.438849585982,-3.36900824102305,330.133562446288));
#13005=CARTESIAN_POINT('Ctrl Pts',(113.431435202141,-3.4968133837742,330.224556072094));
#13006=CARTESIAN_POINT('Ctrl Pts',(113.4240208183,-3.62095233686414,330.320615987477));
#13007=CARTESIAN_POINT('Ctrl Pts',(113.416615191289,-3.74494467442623,330.416562450355));
#13008=CARTESIAN_POINT('Ctrl Pts',(113.409209564279,-3.86527914771921,330.517563066122));
#13009=CARTESIAN_POINT('Ctrl Pts',(113.401803937269,-3.98151805738212,330.623306668129));
#13010=CARTESIAN_POINT('Ctrl Pts',(113.39440543116,-4.09764519719585,330.72894859208));
#13011=CARTESIAN_POINT('Ctrl Pts',(113.387006925051,-4.2096843380371,330.83932417313));
#13012=CARTESIAN_POINT('Ctrl Pts',(113.379608418942,-4.31722926740279,330.954080819495));
#13013=CARTESIAN_POINT('Ctrl Pts',(113.372215403487,-4.42469438442869,331.068752301487));
#13014=CARTESIAN_POINT('Ctrl Pts',(113.364822388033,-4.52767167589312,331.187798103269));
#13015=CARTESIAN_POINT('Ctrl Pts',(113.357429372579,-4.62579045397227,331.310827567267));
#13016=CARTESIAN_POINT('Ctrl Pts',(113.350040221933,-4.72385793900427,331.433792715787));
#13017=CARTESIAN_POINT('Ctrl Pts',(113.342651071288,-4.81707173594637,331.56073708731));
#13018=CARTESIAN_POINT('Ctrl Pts',(113.335261920642,-4.90510035289923,331.691235715484));
#13019=CARTESIAN_POINT('Ctrl Pts',(113.327873945515,-4.9931149656312,331.821713583005));
#13020=CARTESIAN_POINT('Ctrl Pts',(113.320485970388,-5.07594582606789,331.955744275184));
#13021=CARTESIAN_POINT('Ctrl Pts',(113.313097995262,-5.15330378174896,332.092872432192));
#13022=CARTESIAN_POINT('Ctrl Pts',(113.305710294204,-5.23065886770477,332.229995502196));
#13023=CARTESIAN_POINT('Ctrl Pts',(113.298322593147,-5.30254126861194,332.370215482582));
#13024=CARTESIAN_POINT('Ctrl Pts',(113.29093489209,-5.36870711185131,332.513051164648));
#13025=CARTESIAN_POINT('Ctrl Pts',(113.283545996999,-5.43488364910755,332.65590993245));
#13026=CARTESIAN_POINT('Ctrl Pts',(113.276157101909,-5.49534163183526,332.801384903988));
#13027=CARTESIAN_POINT('Ctrl Pts',(113.268768206819,-5.54988485107399,332.948973744117));
#13028=CARTESIAN_POINT('Ctrl Pts',(113.261376649147,-5.60444772491199,333.096615767751));
#13029=CARTESIAN_POINT('Ctrl Pts',(113.253985091475,-5.653091462294,333.246372825637));
#13030=CARTESIAN_POINT('Ctrl Pts',(113.246593533803,-5.69566939665332,333.397726400852));
#13031=CARTESIAN_POINT('Ctrl Pts',(113.239193853586,-5.73829411968817,333.549246297741));
#13032=CARTESIAN_POINT('Ctrl Pts',(113.231794173369,-5.7748396276477,333.702365854845));
#13033=CARTESIAN_POINT('Ctrl Pts',(113.224394493152,-5.80521000822408,333.856554626178));
#13034=CARTESIAN_POINT('Ctrl Pts',(113.216990175569,-5.835599421864,334.01084002734));
#13035=CARTESIAN_POINT('Ctrl Pts',(113.209585857985,-5.8598059399352,334.16619560897));
#13036=CARTESIAN_POINT('Ctrl Pts',(113.202181540402,-5.87778548397389,334.322085280521));
#13037=CARTESIAN_POINT('Ctrl Pts',(113.194766836303,-5.89579024908249,334.478193628603));
#13038=CARTESIAN_POINT('Ctrl Pts',(113.187352132204,-5.90755056919457,334.634837190683));
#13039=CARTESIAN_POINT('Ctrl Pts',(113.179937428105,-5.91307444445758,334.791478593898));
#13040=CARTESIAN_POINT('Ctrl Pts',(113.176642286971,-5.91552928936512,334.861091018633));
#13041=CARTESIAN_POINT('Ctrl Pts',(113.173347145837,-5.91675314398094,334.930703063999));
#13042=CARTESIAN_POINT('Ctrl Pts',(113.170052004703,-5.91674999393393,335.000267923214));
#13043=CARTESIAN_POINT('',(111.420052816644,-5.91485974286145,334.994705964346));
#13044=CARTESIAN_POINT('Ctrl Pts',(113.170052004703,-5.92648485094407,335.000268364029));
#13045=CARTESIAN_POINT('Ctrl Pts',(113.169376648319,-5.92649426041998,335.014549503925));
#13046=CARTESIAN_POINT('Ctrl Pts',(113.168701291934,-5.92644711627134,335.028830579886));
#13047=CARTESIAN_POINT('Ctrl Pts',(113.168025935549,-5.92634323144412,335.043111243086));
#13048=CARTESIAN_POINT('Ctrl Pts',(113.075279924124,-5.91207683285968,337.00426032246));
#13049=CARTESIAN_POINT('Ctrl Pts',(112.889787901276,-3.74337052513098,340.910989767612));
#13050=CARTESIAN_POINT('Ctrl Pts',(112.611549867001,2.94492481531614,341.346655871666));
#13051=CARTESIAN_POINT('Ctrl Pts',(112.333311832728,6.93070611976698,335.95808955878));
#13052=CARTESIAN_POINT('Ctrl Pts',(112.055073798453,4.55628071516118,329.690298599179));
#13053=CARTESIAN_POINT('Ctrl Pts',(111.776835764179,-1.99937625115185,328.29514224405));
#13054=CARTESIAN_POINT('Ctrl Pts',(111.565162248396,-5.59083635352281,331.914700220535));
#13055=CARTESIAN_POINT('Ctrl Pts',(111.446234744037,-5.91862083319085,334.437990101302));
#13056=CARTESIAN_POINT('Ctrl Pts',(111.420053251102,-5.91384955313574,334.994697627575));
#13057=CARTESIAN_POINT('',(109.670051150406,-5.91183323294406,335.00229756853));
#13058=CARTESIAN_POINT('Ctrl Pts',(111.420052004703,-5.91674764548976,334.994721544598));
#13059=CARTESIAN_POINT('Ctrl Pts',(111.412711157276,-5.91688696497021,335.150888101892));
#13060=CARTESIAN_POINT('Ctrl Pts',(111.40537030985,-5.91083926829776,335.307182781746));
#13061=CARTESIAN_POINT('Ctrl Pts',(111.398029462423,-5.8986010122119,335.463073062521));
#13062=CARTESIAN_POINT('Ctrl Pts',(111.390626555473,-5.88625929391097,335.620281239706));
#13063=CARTESIAN_POINT('Ctrl Pts',(111.383223648524,-5.86762182953684,335.777077758205));
#13064=CARTESIAN_POINT('Ctrl Pts',(111.375820741574,-5.84273868919298,335.932917559223));
#13065=CARTESIAN_POINT('Ctrl Pts',(111.368484115834,-5.81807833763348,336.087362063694));
#13066=CARTESIAN_POINT('Ctrl Pts',(111.361147490094,-5.7872837741526,336.240866533846));
#13067=CARTESIAN_POINT('Ctrl Pts',(111.353810864354,-5.75045564278118,336.392907198239));
#13068=CARTESIAN_POINT('Ctrl Pts',(111.346474105685,-5.71362684413768,336.544950617387));
#13069=CARTESIAN_POINT('Ctrl Pts',(111.339137347016,-5.67076434911301,336.695529808621));
#13070=CARTESIAN_POINT('Ctrl Pts',(111.331800588347,-5.62201945940217,336.844133335907));
#13071=CARTESIAN_POINT('Ctrl Pts',(111.324462190267,-5.57326367756963,336.992770068883));
#13072=CARTESIAN_POINT('Ctrl Pts',(111.317123792188,-5.51862300344348,337.139429898357));
#13073=CARTESIAN_POINT('Ctrl Pts',(111.309785394109,-5.45829785252835,337.283618863905));
#13074=CARTESIAN_POINT('Ctrl Pts',(111.302333252569,-5.39703767582811,337.430042724828));
#13075=CARTESIAN_POINT('Ctrl Pts',(111.294881111029,-5.32991549936494,337.573918115048));
#13076=CARTESIAN_POINT('Ctrl Pts',(111.287428969489,-5.25719048201953,337.714752069391));
#13077=CARTESIAN_POINT('Ctrl Pts',(111.280079056957,-5.18546311163429,337.853654053532));
#13078=CARTESIAN_POINT('Ctrl Pts',(111.272729144425,-5.10828588806572,337.989597218341));
#13079=CARTESIAN_POINT('Ctrl Pts',(111.265379231893,-5.02595180002468,338.122136939074));
#13080=CARTESIAN_POINT('Ctrl Pts',(111.257875975849,-4.94189995029351,338.257441877228));
#13081=CARTESIAN_POINT('Ctrl Pts',(111.250372719806,-4.85247393290783,338.389199448089));
#13082=CARTESIAN_POINT('Ctrl Pts',(111.242869463762,-4.75802902184952,338.516971764137));
#13083=CARTESIAN_POINT('Ctrl Pts',(111.235366207718,-4.66358411079121,338.644744080186));
#13084=CARTESIAN_POINT('Ctrl Pts',(111.227862951675,-4.56412061731915,338.768530860917));
#13085=CARTESIAN_POINT('Ctrl Pts',(111.220359695631,-4.46003343831345,338.887934193325));
#13086=CARTESIAN_POINT('Ctrl Pts',(111.212935718193,-4.35704603337513,339.006075922817));
#13087=CARTESIAN_POINT('Ctrl Pts',(111.205511740755,-4.24920584456463,339.120301002308));
#13088=CARTESIAN_POINT('Ctrl Pts',(111.198087763317,-4.1368422863769,339.230185156721));
#13089=CARTESIAN_POINT('Ctrl Pts',(111.190672547289,-4.02461133409392,339.339939631299));
#13090=CARTESIAN_POINT('Ctrl Pts',(111.183257331262,-3.90786790255102,339.445363119701));
#13091=CARTESIAN_POINT('Ctrl Pts',(111.175842115234,-3.78698156412167,339.546064363326));
#13092=CARTESIAN_POINT('Ctrl Pts',(111.16843403409,-3.66621154191839,339.646668712722));
#13093=CARTESIAN_POINT('Ctrl Pts',(111.161025952946,-3.54130683361324,339.742559625765));
#13094=CARTESIAN_POINT('Ctrl Pts',(111.153617871802,-3.41267367717123,339.833382763204));
#13095=CARTESIAN_POINT('Ctrl Pts',(111.146215304628,-3.28413626473679,339.924138299324));
#13096=CARTESIAN_POINT('Ctrl Pts',(111.138812737454,-3.15187623346712,340.009833356178));
#13097=CARTESIAN_POINT('Ctrl Pts',(111.13141017028,-3.0163326121967,340.090154038445));
#13098=CARTESIAN_POINT('Ctrl Pts',(111.124011500525,-2.88086035405,340.170432432224));
#13099=CARTESIAN_POINT('Ctrl Pts',(111.11661283077,-2.7421082691653,340.245341896921));
#13100=CARTESIAN_POINT('Ctrl Pts',(111.109214161016,-2.60054396129825,340.314612090064));
#13101=CARTESIAN_POINT('Ctrl Pts',(111.101816711812,-2.4590030071468,340.383870855776));
#13102=CARTESIAN_POINT('Ctrl Pts',(111.094419262608,-2.31465108566736,340.447492032413));
#13103=CARTESIAN_POINT('Ctrl Pts',(111.087021813404,-2.16798007681421,340.505251397442));
#13104=CARTESIAN_POINT('Ctrl Pts',(111.07962468494,-2.0213154273601,340.563008258125));
#13105=CARTESIAN_POINT('Ctrl Pts',(111.072227556477,-1.87233223771711,340.6149036758));
#13106=CARTESIAN_POINT('Ctrl Pts',(111.064830428013,-1.72154177321008,340.660761829082));
#13107=CARTESIAN_POINT('Ctrl Pts',(111.057432160577,-1.57072809073576,340.706627043375));
#13108=CARTESIAN_POINT('Ctrl Pts',(111.05003389314,-1.41810693640083,340.746453033746));
#13109=CARTESIAN_POINT('Ctrl Pts',(111.042635625704,-1.26420397032278,340.780114089179));
#13110=CARTESIAN_POINT('Ctrl Pts',(111.035234759178,-1.11024693651417,340.813786970094));
#13111=CARTESIAN_POINT('Ctrl Pts',(111.027833892652,-0.955007558751131,
340.84129052426));
#13112=CARTESIAN_POINT('Ctrl Pts',(111.020433026126,-0.79902075118346,340.86255033255));
#13113=CARTESIAN_POINT('Ctrl Pts',(111.013024032742,-0.642862655188266,
340.883833486141));
#13114=CARTESIAN_POINT('Ctrl Pts',(111.005615039357,-0.485955860321188,
340.898859151168));
#13115=CARTESIAN_POINT('Ctrl Pts',(110.998206045972,-0.328840188593058,
340.90760481861));
#13116=CARTESIAN_POINT('Ctrl Pts',(110.990792488392,-0.171627728191757,
340.916355873685));
#13117=CARTESIAN_POINT('Ctrl Pts',(110.983378930812,-0.0142065068204832,
340.918819216462));
#13118=CARTESIAN_POINT('Ctrl Pts',(110.975965373231,0.142885120426389,340.915024463589));
#13119=CARTESIAN_POINT('Ctrl Pts',(110.968541261095,0.300200396364228,340.911224308191));
#13120=CARTESIAN_POINT('Ctrl Pts',(110.961117148958,0.457184769575989,340.90114828684));
#13121=CARTESIAN_POINT('Ctrl Pts',(110.953693036821,0.61330563832227,340.884877803022));
#13122=CARTESIAN_POINT('Ctrl Pts',(110.949835911667,0.694416715164889,340.876424631619));
#13123=CARTESIAN_POINT('Ctrl Pts',(110.945978786512,0.775294879731979,340.866300280802));
#13124=CARTESIAN_POINT('Ctrl Pts',(110.942121661357,0.855866798469,340.854521550543));
#13125=CARTESIAN_POINT('Ctrl Pts',(110.934697683919,1.01094709347015,340.83185051339));
#13126=CARTESIAN_POINT('Ctrl Pts',(110.927273706481,1.16535991373322,340.802979142696));
#13127=CARTESIAN_POINT('Ctrl Pts',(110.919849729043,1.31857021221013,340.767954850549));
#13128=CARTESIAN_POINT('Ctrl Pts',(110.912434513016,1.47159969948322,340.732971892337));
#13129=CARTESIAN_POINT('Ctrl Pts',(110.905019296988,1.62342912953639,340.691850548913));
#13130=CARTESIAN_POINT('Ctrl Pts',(110.897604080961,1.77352948784842,340.644689869092));
#13131=CARTESIAN_POINT('Ctrl Pts',(110.890195999816,1.92348542035144,340.59757456704));
#13132=CARTESIAN_POINT('Ctrl Pts',(110.882787918672,2.07171523956719,340.544431608368));
#13133=CARTESIAN_POINT('Ctrl Pts',(110.875379837528,2.2177011353867,340.485410853947));
#13134=CARTESIAN_POINT('Ctrl Pts',(110.867977270354,2.36357837123802,340.426434029752));
#13135=CARTESIAN_POINT('Ctrl Pts',(110.86057470318,2.50721466476932,340.361588260258));
#13136=CARTESIAN_POINT('Ctrl Pts',(110.853172136006,2.6481084710155,340.291072867409));
#13137=CARTESIAN_POINT('Ctrl Pts',(110.845773466251,2.78892809728785,340.220594600608));
#13138=CARTESIAN_POINT('Ctrl Pts',(110.838374796497,2.92700777899786,340.144452821934));
#13139=CARTESIAN_POINT('Ctrl Pts',(110.830976126742,3.06186713217097,340.06289445154));
#13140=CARTESIAN_POINT('Ctrl Pts',(110.823578677538,3.19670423773869,339.981349535744));
#13141=CARTESIAN_POINT('Ctrl Pts',(110.816181228334,3.32832175009543,339.894389994619));
#13142=CARTESIAN_POINT('Ctrl Pts',(110.80878377913,3.45626493126137,339.802308120834));
#13143=CARTESIAN_POINT('Ctrl Pts',(110.801386650667,3.58420256503402,339.710230239559));
#13144=CARTESIAN_POINT('Ctrl Pts',(110.793989522203,3.70846588146624,339.613030685234));
#13145=CARTESIAN_POINT('Ctrl Pts',(110.78659239374,3.82863035360154,339.511044244738));
#13146=CARTESIAN_POINT('Ctrl Pts',(110.779194126303,3.94881332806575,339.409042100876));
#13147=CARTESIAN_POINT('Ctrl Pts',(110.771795858866,4.06489591702984,339.302251844771));
#13148=CARTESIAN_POINT('Ctrl Pts',(110.76439759143,4.17648794256494,339.191047485786));
#13149=CARTESIAN_POINT('Ctrl Pts',(110.756996724904,4.28811917155207,339.07980405954));
#13150=CARTESIAN_POINT('Ctrl Pts',(110.749595858378,4.39525643195436,338.964143706205));
#13151=CARTESIAN_POINT('Ctrl Pts',(110.742194991853,4.49754767039888,338.844475974042));
#13152=CARTESIAN_POINT('Ctrl Pts',(110.734785998468,4.59995123440293,338.724676835269));
#13153=CARTESIAN_POINT('Ctrl Pts',(110.727377005083,4.69749790669539,338.600861813524));
#13154=CARTESIAN_POINT('Ctrl Pts',(110.719968011698,4.78987663029553,338.473472675731));
#13155=CARTESIAN_POINT('Ctrl Pts',(110.712554454118,4.88231226237568,338.346005061835));
#13156=CARTESIAN_POINT('Ctrl Pts',(110.705140896538,4.96957339558215,338.214959254473));
#13157=CARTESIAN_POINT('Ctrl Pts',(110.697727338957,5.0513936003527,338.080803995196));
#13158=CARTESIAN_POINT('Ctrl Pts',(110.690303226821,5.13333029116406,337.946457741347));
#13159=CARTESIAN_POINT('Ctrl Pts',(110.682879114684,5.20981040195362,337.808993519483));
#13160=CARTESIAN_POINT('Ctrl Pts',(110.675455002547,5.28061416528821,337.668903257868));
#13161=CARTESIAN_POINT('Ctrl Pts',(110.671597877393,5.31739957094704,337.596120726832));
#13162=CARTESIAN_POINT('Ctrl Pts',(110.667740752238,5.35265360398758,337.522629685625));
#13163=CARTESIAN_POINT('Ctrl Pts',(110.663883627083,5.38635070686979,337.448500893425));
#13164=CARTESIAN_POINT('Ctrl Pts',(110.656459649645,5.45120899419265,337.305821965798));
#13165=CARTESIAN_POINT('Ctrl Pts',(110.649035672207,5.51049207988238,337.160348975664));
#13166=CARTESIAN_POINT('Ctrl Pts',(110.641611694769,5.56395028911653,337.012557512902));
#13167=CARTESIAN_POINT('Ctrl Pts',(110.634196478742,5.61734540962053,336.864940466303));
#13168=CARTESIAN_POINT('Ctrl Pts',(110.626781262714,5.66492921122269,336.715010740964));
#13169=CARTESIAN_POINT('Ctrl Pts',(110.619366046686,5.70649870607189,336.563266797479));
#13170=CARTESIAN_POINT('Ctrl Pts',(110.611957965542,5.74802820296249,336.411668861252));
#13171=CARTESIAN_POINT('Ctrl Pts',(110.604549884398,5.78355481586299,336.258260539649));
#13172=CARTESIAN_POINT('Ctrl Pts',(110.597141803254,5.81292434921464,336.103558368555));
#13173=CARTESIAN_POINT('Ctrl Pts',(110.58973923608,5.84227202228622,335.948971345112));
#13174=CARTESIAN_POINT('Ctrl Pts',(110.582336668906,5.86547167157338,335.793092754813));
#13175=CARTESIAN_POINT('Ctrl Pts',(110.574934101732,5.88241949639207,335.636452222061));
#13176=CARTESIAN_POINT('Ctrl Pts',(110.567535431977,5.89935839825507,335.479894159865));
#13177=CARTESIAN_POINT('Ctrl Pts',(110.560136762223,5.91005199093873,335.322575324259));
#13178=CARTESIAN_POINT('Ctrl Pts',(110.552738092468,5.9144479515326,335.165033303039));
#13179=CARTESIAN_POINT('Ctrl Pts',(110.545340643264,5.91884318692946,335.00751727136));
#13180=CARTESIAN_POINT('Ctrl Pts',(110.53794319406,5.91694284174497,334.849778499843));
#13181=CARTESIAN_POINT('Ctrl Pts',(110.530545744856,5.90874662630595,334.692357563691));
#13182=CARTESIAN_POINT('Ctrl Pts',(110.523148616393,5.90055076624054,334.534943453037));
#13183=CARTESIAN_POINT('Ctrl Pts',(110.515751487929,5.88605959809588,334.377847523053));
#13184=CARTESIAN_POINT('Ctrl Pts',(110.508354359466,5.8653249154058,334.221607939904));
#13185=CARTESIAN_POINT('Ctrl Pts',(110.500956092029,5.84458704009223,334.065344299761));
#13186=CARTESIAN_POINT('Ctrl Pts',(110.493557824592,5.81760378516971,333.909937638986));
#13187=CARTESIAN_POINT('Ctrl Pts',(110.486159557156,5.7844785154243,333.755918464451));
#13188=CARTESIAN_POINT('Ctrl Pts',(110.47875869063,5.75134160842319,333.601845181359));
#13189=CARTESIAN_POINT('Ctrl Pts',(110.471357824104,5.71205846893741,333.449160719635));
#13190=CARTESIAN_POINT('Ctrl Pts',(110.463956957579,5.66678297855492,333.298382758532));
#13191=CARTESIAN_POINT('Ctrl Pts',(110.456547964194,5.62145777135548,333.147439228814));
#13192=CARTESIAN_POINT('Ctrl Pts',(110.449138970809,5.57012717969713,332.998406738246));
#13193=CARTESIAN_POINT('Ctrl Pts',(110.441729977424,5.51299436402923,332.85178592671));
#13194=CARTESIAN_POINT('Ctrl Pts',(110.434316419844,5.45582635257627,332.705074791697));
#13195=CARTESIAN_POINT('Ctrl Pts',(110.426902862264,5.39284914364688,332.560778637379));
#13196=CARTESIAN_POINT('Ctrl Pts',(110.419489304684,5.32431273168775,332.419375173008));
#13197=CARTESIAN_POINT('Ctrl Pts',(110.412065192547,5.25567874559884,332.277770394918));
#13198=CARTESIAN_POINT('Ctrl Pts',(110.40464108041,5.18146992513943,332.139066859978));
#13199=CARTESIAN_POINT('Ctrl Pts',(110.397216968274,5.10198101451226,332.00371558592));
#13200=CARTESIAN_POINT('Ctrl Pts',(110.393359843119,5.06068332516423,331.933395149714));
#13201=CARTESIAN_POINT('Ctrl Pts',(110.389502717964,5.01796112090388,331.863979061905));
#13202=CARTESIAN_POINT('Ctrl Pts',(110.385645592809,4.97386007398293,331.795527106225));
#13203=CARTESIAN_POINT('Ctrl Pts',(110.378221615371,4.88897686065786,331.66377463407));
#13204=CARTESIAN_POINT('Ctrl Pts',(110.370797637933,4.79872699905348,331.535198440364));
#13205=CARTESIAN_POINT('Ctrl Pts',(110.363373660495,4.70337530947232,331.410265850965));
#13206=CARTESIAN_POINT('Ctrl Pts',(110.355958444468,4.60813614923138,331.285480700819));
#13207=CARTESIAN_POINT('Ctrl Pts',(110.34854322844,4.50780736998794,331.164330889549));
#13208=CARTESIAN_POINT('Ctrl Pts',(110.341128012412,4.40269828951588,331.047256859598));
#13209=CARTESIAN_POINT('Ctrl Pts',(110.333719931268,4.2976903444719,330.93029547769));
#13210=CARTESIAN_POINT('Ctrl Pts',(110.326311850124,4.18791150277028,330.817402345588));
#13211=CARTESIAN_POINT('Ctrl Pts',(110.31890376898,4.07371268639084,330.708986656833));
#13212=CARTESIAN_POINT('Ctrl Pts',(110.311501201806,3.95959887027595,330.600651663855));
#13213=CARTESIAN_POINT('Ctrl Pts',(110.304098634632,3.8410718995945,330.496787734304));
#13214=CARTESIAN_POINT('Ctrl Pts',(110.296696067458,3.71852097429914,330.397768766544));
#13215=CARTESIAN_POINT('Ctrl Pts',(110.289297397703,3.59603457153095,330.298801931838));
#13216=CARTESIAN_POINT('Ctrl Pts',(110.281898727949,3.46952872301975,330.204675212714));
#13217=CARTESIAN_POINT('Ctrl Pts',(110.274500058194,3.33942718288179,330.115723528225));
#13218=CARTESIAN_POINT('Ctrl Pts',(110.26710260899,3.20934710545753,330.026786518003));
#13219=CARTESIAN_POINT('Ctrl Pts',(110.259705159786,3.07567282145844,329.943023058494));
#13220=CARTESIAN_POINT('Ctrl Pts',(110.252307710582,2.93885875534673,329.864725929551));
#13221=CARTESIAN_POINT('Ctrl Pts',(110.244910582118,2.80205062125432,329.786432195436));
#13222=CARTESIAN_POINT('Ctrl Pts',(110.237513453655,2.66210329964956,329.713604506008));
#13223=CARTESIAN_POINT('Ctrl Pts',(110.230116325192,2.51949737439505,329.64649053957));
#13224=CARTESIAN_POINT('Ctrl Pts',(110.222718057755,2.37686949138777,329.579366239256));
#13225=CARTESIAN_POINT('Ctrl Pts',(110.215319790318,2.23158252734815,329.517957572605));
#13226=CARTESIAN_POINT('Ctrl Pts',(110.207921522882,2.08413853343867,329.462464705671));
#13227=CARTESIAN_POINT('Ctrl Pts',(110.200520656356,1.93664274090411,329.40695234351));
#13228=CARTESIAN_POINT('Ctrl Pts',(110.19311978983,1.78698875881798,329.357360050301));
#13229=CARTESIAN_POINT('Ctrl Pts',(110.185718923304,1.63569518886718,329.313838569684));
#13230=CARTESIAN_POINT('Ctrl Pts',(110.17830992992,1.48423548411169,329.27026929832));
#13231=CARTESIAN_POINT('Ctrl Pts',(110.170900936535,1.33113295482855,329.232784255807));
#13232=CARTESIAN_POINT('Ctrl Pts',(110.16349194315,1.17691854155148,329.201483525155));
#13233=CARTESIAN_POINT('Ctrl Pts',(110.15607838557,1.02260912687707,329.170163512173));
#13234=CARTESIAN_POINT('Ctrl Pts',(110.14866482799,0.867186830903961,329.145035461909));
#13235=CARTESIAN_POINT('Ctrl Pts',(110.141251270409,0.711188655873953,329.126147664585));
#13236=CARTESIAN_POINT('Ctrl Pts',(110.133827158273,0.55496838888195,329.107232977025));
#13237=CARTESIAN_POINT('Ctrl Pts',(110.126403046136,0.398170976388124,329.094576315762));
#13238=CARTESIAN_POINT('Ctrl Pts',(110.118978933999,0.241335191826657,329.088173895683));
#13239=CARTESIAN_POINT('Ctrl Pts',(110.115121808845,0.159852687435522,329.084847580686));
#13240=CARTESIAN_POINT('Ctrl Pts',(110.11126468369,0.0783597821473199,329.083208565479));
#13241=CARTESIAN_POINT('Ctrl Pts',(110.107407558535,-0.00306853474573501,
329.083250795699));
#13242=CARTESIAN_POINT('Ctrl Pts',(110.099983581097,-0.159797176724483,
329.08333207805));
#13243=CARTESIAN_POINT('Ctrl Pts',(110.092559603659,-0.316759019714356,
329.089645155955));
#13244=CARTESIAN_POINT('Ctrl Pts',(110.085135626221,-0.473417769970754,
329.102220233208));
#13245=CARTESIAN_POINT('Ctrl Pts',(110.077720410194,-0.629891639330824,
329.114780469979));
#13246=CARTESIAN_POINT('Ctrl Pts',(110.070305194166,-0.7860627595581,329.133587966412));
#13247=CARTESIAN_POINT('Ctrl Pts',(110.062889978138,-0.941393363609252,
329.158620959272));
#13248=CARTESIAN_POINT('Ctrl Pts',(110.055481896994,-1.09657450933539,329.183629865513));
#13249=CARTESIAN_POINT('Ctrl Pts',(110.04807381585,-1.2509163829423,329.214852283941));
#13250=CARTESIAN_POINT('Ctrl Pts',(110.040665734706,-1.4038849808329,329.252214554884));
#13251=CARTESIAN_POINT('Ctrl Pts',(110.033263167532,-1.55673972140211,329.289549016405));
#13252=CARTESIAN_POINT('Ctrl Pts',(110.025860600358,-1.70822286051232,329.333014142722));
#13253=CARTESIAN_POINT('Ctrl Pts',(110.018458033184,-1.85780936062617,329.38248498515));
#13254=CARTESIAN_POINT('Ctrl Pts',(110.011059363429,-2.00731710410265,329.431929781395));
#13255=CARTESIAN_POINT('Ctrl Pts',(110.003660693675,-2.1549298438544,329.487373879585));
#13256=CARTESIAN_POINT('Ctrl Pts',(109.99626202392,-2.3001366216363,329.548642179759));
#13257=CARTESIAN_POINT('Ctrl Pts',(109.988864574716,-2.44531944480805,329.609900372565));
#13258=CARTESIAN_POINT('Ctrl Pts',(109.981467125512,-2.58809675022478,329.676980715509));
#13259=CARTESIAN_POINT('Ctrl Pts',(109.974069676308,-2.72797641791053,329.749659513344));
#13260=CARTESIAN_POINT('Ctrl Pts',(109.966672547844,-2.86785002065765,329.822335159952));
#13261=CARTESIAN_POINT('Ctrl Pts',(109.959275419381,-3.00482590430447,329.900608606733));
#13262=CARTESIAN_POINT('Ctrl Pts',(109.951878290918,-3.13843571937687,329.984209753405));
#13263=CARTESIAN_POINT('Ctrl Pts',(109.944480023481,-3.27206610702601,330.067823772567));
#13264=CARTESIAN_POINT('Ctrl Pts',(109.937081756044,-3.4023290777154,330.156766927036));
#13265=CARTESIAN_POINT('Ctrl Pts',(109.929683488608,-3.52878461884769,330.250725352616));
#13266=CARTESIAN_POINT('Ctrl Pts',(109.922282622082,-3.65528458514079,330.344716786779));
#13267=CARTESIAN_POINT('Ctrl Pts',(109.914881755556,-3.7779741593557,330.443726777582));
#13268=CARTESIAN_POINT('Ctrl Pts',(109.907480889031,-3.89644593282013,330.547400797836));
#13269=CARTESIAN_POINT('Ctrl Pts',(109.900071895646,-4.01504779961826,330.651188662076));
#13270=CARTESIAN_POINT('Ctrl Pts',(109.892662902261,-4.12942233519182,330.759650537854));
#13271=CARTESIAN_POINT('Ctrl Pts',(109.885253908876,-4.2391980552138,330.872394106607));
#13272=CARTESIAN_POINT('Ctrl Pts',(109.877840351296,-4.34904140086573,330.985207129287));
#13273=CARTESIAN_POINT('Ctrl Pts',(109.870426793716,-4.45428003689691,331.102306823915));
#13274=CARTESIAN_POINT('Ctrl Pts',(109.863013236136,-4.55458275230158,331.223267746459));
#13275=CARTESIAN_POINT('Ctrl Pts',(109.855589123999,-4.65502826698499,331.344400879022));
#13276=CARTESIAN_POINT('Ctrl Pts',(109.848165011862,-4.75052360039316,331.469405922665));
#13277=CARTESIAN_POINT('Ctrl Pts',(109.840740899726,-4.84078037428869,331.597827762972));
#13278=CARTESIAN_POINT('Ctrl Pts',(109.836883774571,-4.88767240212476,331.66454807936));
#13279=CARTESIAN_POINT('Ctrl Pts',(109.833026649416,-4.93315117209298,331.732190236817));
#13280=CARTESIAN_POINT('Ctrl Pts',(109.829169524262,-4.97718119442729,331.800687898885));
#13281=CARTESIAN_POINT('Ctrl Pts',(109.821573460546,-5.06389211036479,331.935584378665));
#13282=CARTESIAN_POINT('Ctrl Pts',(109.813977396831,-5.14523351640621,332.074192335918));
#13283=CARTESIAN_POINT('Ctrl Pts',(109.806381333115,-5.2208801338831,332.216056539704));
#13284=CARTESIAN_POINT('Ctrl Pts',(109.798795450889,-5.29642535736611,332.357730593835));
#13285=CARTESIAN_POINT('Ctrl Pts',(109.791209568663,-5.36629083199038,332.502651895537));
#13286=CARTESIAN_POINT('Ctrl Pts',(109.783623686437,-5.43019430910244,332.650336124487));
#13287=CARTESIAN_POINT('Ctrl Pts',(109.776046747252,-5.49402245002688,332.797846247624));
#13288=CARTESIAN_POINT('Ctrl Pts',(109.768469808068,-5.55190245623123,332.948112490534));
#13289=CARTESIAN_POINT('Ctrl Pts',(109.760892868883,-5.60359774706154,333.100625668377));
#13290=CARTESIAN_POINT('Ctrl Pts',(109.753322796868,-5.6552461851559,333.253000619711));
#13291=CARTESIAN_POINT('Ctrl Pts',(109.745752724853,-5.70072095848832,333.407618120489));
#13292=CARTESIAN_POINT('Ctrl Pts',(109.738182652838,-5.73983330636068,333.563948407023));
#13293=CARTESIAN_POINT('Ctrl Pts',(109.730621362071,-5.77890028409332,333.720097351159));
#13294=CARTESIAN_POINT('Ctrl Pts',(109.723060071304,-5.81161947080259,333.877954779919));
#13295=CARTESIAN_POINT('Ctrl Pts',(109.715498780537,-5.83785189284057,334.036975680599));
#13296=CARTESIAN_POINT('Ctrl Pts',(109.707924317898,-5.86413001211656,334.196273597863));
#13297=CARTESIAN_POINT('Ctrl Pts',(109.700349855259,-5.88389864039625,334.356738706662));
#13298=CARTESIAN_POINT('Ctrl Pts',(109.69277539262,-5.89706912905482,334.51781098141));
#13299=CARTESIAN_POINT('Ctrl Pts',(109.685200929981,-5.91023961771339,334.678883256159));
#13300=CARTESIAN_POINT('Ctrl Pts',(109.677626467342,-5.9168119122902,334.840562346074));
#13301=CARTESIAN_POINT('Ctrl Pts',(109.670052004703,-5.91674956022219,335.00228125196));
#13302=CARTESIAN_POINT('',(107.920052004703,-5.92221754830578,335.00433605404));
#13303=CARTESIAN_POINT('Ctrl Pts',(109.670050448713,-5.90779511345791,335.002310970458));
#13304=CARTESIAN_POINT('Ctrl Pts',(109.630344129138,-5.91071301687524,335.848780750068));
#13305=CARTESIAN_POINT('Ctrl Pts',(109.497891798137,-5.34435609359717,338.668701282137));
#13306=CARTESIAN_POINT('Ctrl Pts',(109.272693455716,-1.00488954949076,341.924075383365));
#13307=CARTESIAN_POINT('Ctrl Pts',(108.99445542144,5.27879931276318,339.592047553848));
#13308=CARTESIAN_POINT('Ctrl Pts',(108.716217387167,6.71821196064523,333.045965462669));
#13309=CARTESIAN_POINT('Ctrl Pts',(108.437979352892,1.99242065288906,328.293072024904));
#13310=CARTESIAN_POINT('Ctrl Pts',(108.172590892072,-4.2590996869207,329.630282370671));
#13311=CARTESIAN_POINT('Ctrl Pts',(107.999948442675,-5.90829782333765,333.311624078754));
#13312=CARTESIAN_POINT('Ctrl Pts',(107.920052004703,-5.92221754830578,335.00433605404));
#13313=CARTESIAN_POINT('',(106.170052004703,-5.92154411674314,334.995412275155));
#13314=CARTESIAN_POINT('Ctrl Pts',(107.920052004703,-5.92221754830578,335.00433605404));
#13315=CARTESIAN_POINT('Ctrl Pts',(107.90720243125,-5.92445622793863,335.276571305242));
#13316=CARTESIAN_POINT('Ctrl Pts',(107.801606846373,-5.78358165308998,337.511424151982));
#13317=CARTESIAN_POINT('Ctrl Pts',(107.60326525007,-2.93834024845692,341.349707040925));
#13318=CARTESIAN_POINT('Ctrl Pts',(107.325027215796,3.74949960540118,340.907103827622));
#13319=CARTESIAN_POINT('Ctrl Pts',(107.046789181522,6.996479013907,335.043638620423));
#13320=CARTESIAN_POINT('Ctrl Pts',(106.768551147248,3.82289289921021,329.14012689537));
#13321=CARTESIAN_POINT('Ctrl Pts',(106.490313112974,-2.85890560328287,328.614134226846));
#13322=CARTESIAN_POINT('Ctrl Pts',(106.290813398793,-5.76869590651112,332.438829820194));
#13323=CARTESIAN_POINT('Ctrl Pts',(106.184059696036,-5.92408171522026,334.698552889316));
#13324=CARTESIAN_POINT('Ctrl Pts',(106.170052004703,-5.92154411674314,334.995412275155));
#13325=CARTESIAN_POINT('',(104.42005273448,-5.91170307006019,334.998082814567));
#13326=CARTESIAN_POINT('Ctrl Pts',(106.170052004703,-5.92154411674314,334.995412275155));
#13327=CARTESIAN_POINT('Ctrl Pts',(106.091313684611,-5.90728007876455,336.664081921709));
#13328=CARTESIAN_POINT('Ctrl Pts',(105.919829353095,-4.29854415330596,340.322347225061));
#13329=CARTESIAN_POINT('Ctrl Pts',(105.655599010152,1.90860364104225,341.731259545033));
#13330=CARTESIAN_POINT('Ctrl Pts',(105.377360975878,6.69331470236746,337.037685259384));
#13331=CARTESIAN_POINT('Ctrl Pts',(105.099122941604,5.33566965449091,330.474157287383));
#13332=CARTESIAN_POINT('Ctrl Pts',(104.820884907332,-0.918440680953387,
328.06392837142));
#13333=CARTESIAN_POINT('Ctrl Pts',(104.594528372549,-5.32070196082337,331.281381489484));
#13334=CARTESIAN_POINT('Ctrl Pts',(104.46091784919,-5.91003360597982,334.126814980488));
#13335=CARTESIAN_POINT('Ctrl Pts',(104.420053337258,-5.90753467241241,334.998071303833));
#13336=CARTESIAN_POINT('',(102.670051327749,-5.91521396419827,335.005380775613));
#13337=CARTESIAN_POINT('Ctrl Pts',(104.420052004704,-5.91674969388947,334.99809675046));
#13338=CARTESIAN_POINT('Ctrl Pts',(104.412468296942,-5.91680178579455,335.160038081326));
#13339=CARTESIAN_POINT('Ctrl Pts',(104.404884589181,-5.9102010264601,335.321923755964));
#13340=CARTESIAN_POINT('Ctrl Pts',(104.397300881419,-5.8969874206776,335.483187254458));
#13341=CARTESIAN_POINT('Ctrl Pts',(104.389712803173,-5.8837661999047,335.644543688975));
#13342=CARTESIAN_POINT('Ctrl Pts',(104.382124724926,-5.86392456237403,335.805276887542));
#13343=CARTESIAN_POINT('Ctrl Pts',(104.37453664668,-5.83755426134891,335.964826828144));
#13344=CARTESIAN_POINT('Ctrl Pts',(104.366943043201,-5.81116475888245,336.124492944471));
#13345=CARTESIAN_POINT('Ctrl Pts',(104.359349439722,-5.77823717070347,336.282973743893));
#13346=CARTESIAN_POINT('Ctrl Pts',(104.351755836244,-5.73891412015043,336.439720557622));
#13347=CARTESIAN_POINT('Ctrl Pts',(104.344149881205,-5.69952710773525,336.596722331683));
#13348=CARTESIAN_POINT('Ctrl Pts',(104.336543926166,-5.6537239278541,336.751984147316));
#13349=CARTESIAN_POINT('Ctrl Pts',(104.328937971128,-5.60169717914256,336.904972250634));
#13350=CARTESIAN_POINT('Ctrl Pts',(104.321325502156,-5.54962587340528,337.05809137684));
#13351=CARTESIAN_POINT('Ctrl Pts',(104.313713033185,-5.49132049193872,337.208932584453));
#13352=CARTESIAN_POINT('Ctrl Pts',(104.306100564214,-5.42702137540082,337.356983146618));
#13353=CARTESIAN_POINT('Ctrl Pts',(104.298473877911,-5.36260217142819,337.50531021355));
#13354=CARTESIAN_POINT('Ctrl Pts',(104.290847191608,-5.29216700613838,337.650835904882));
#13355=CARTESIAN_POINT('Ctrl Pts',(104.283220505305,-5.21600242325113,337.793071657358));
#13356=CARTESIAN_POINT('Ctrl Pts',(104.276949949798,-5.15338096149142,337.91001591671));
#13357=CARTESIAN_POINT('Ctrl Pts',(104.27067939429,-5.0868873502845,338.02473664031));
#13358=CARTESIAN_POINT('Ctrl Pts',(104.264408838783,-5.01670206739496,338.136977993148));
#13359=CARTESIAN_POINT('Ctrl Pts',(104.256984861345,-4.93360672503615,338.269865305942));
#13360=CARTESIAN_POINT('Ctrl Pts',(104.249560883907,-4.84510230919647,338.39964913962));
#13361=CARTESIAN_POINT('Ctrl Pts',(104.242136906469,-4.75144730191213,338.525858632965));
#13362=CARTESIAN_POINT('Ctrl Pts',(104.234721690441,-4.65790282162755,338.651919180118));
#13363=CARTESIAN_POINT('Ctrl Pts',(104.227306474414,-4.55922006943336,338.774413486658));
#13364=CARTESIAN_POINT('Ctrl Pts',(104.219891258386,-4.45570238400033,338.892896971115));
#13365=CARTESIAN_POINT('Ctrl Pts',(104.212483177242,-4.35228430276294,339.01126645136));
#13366=CARTESIAN_POINT('Ctrl Pts',(104.205075096098,-4.2440407937584,339.125632513281));
#13367=CARTESIAN_POINT('Ctrl Pts',(104.197667014954,-4.13131721827334,339.235581259343));
#13368=CARTESIAN_POINT('Ctrl Pts',(104.19026444778,-4.01867754500458,339.345448168545));
#13369=CARTESIAN_POINT('Ctrl Pts',(104.182861880606,-3.90156471094392,339.450904049076));
#13370=CARTESIAN_POINT('Ctrl Pts',(104.175459313432,-3.78036282873408,339.551569778178));
#13371=CARTESIAN_POINT('Ctrl Pts',(104.168060643677,-3.65922475878535,339.652182507214));
#13372=CARTESIAN_POINT('Ctrl Pts',(104.160661973923,-3.53400221462441,339.748009869666));
#13373=CARTESIAN_POINT('Ctrl Pts',(104.153263304168,-3.40511438655748,339.838711251662));
#13374=CARTESIAN_POINT('Ctrl Pts',(104.145865854964,-3.27624782097983,339.929397670746));
#13375=CARTESIAN_POINT('Ctrl Pts',(104.13846840576,-3.143717476462,340.014959573095));
#13376=CARTESIAN_POINT('Ctrl Pts',(104.131070956556,-3.00797378020425,340.095098065799));
#13377=CARTESIAN_POINT('Ctrl Pts',(104.123673828092,-2.87223596955661,340.175233083837));
#13378=CARTESIAN_POINT('Ctrl Pts',(104.116276699629,-2.7332854055776,340.249944970051));
#13379=CARTESIAN_POINT('Ctrl Pts',(104.108879571166,-2.59159928185225,340.31897957552));
#13380=CARTESIAN_POINT('Ctrl Pts',(104.101481303729,-2.44989134200062,340.388024810596));
#13381=CARTESIAN_POINT('Ctrl Pts',(104.094083036292,-2.30544733924833,340.451390860879));
#13382=CARTESIAN_POINT('Ctrl Pts',(104.086684768856,-2.15876657446428,340.508870795315));
#13383=CARTESIAN_POINT('Ctrl Pts',(104.07928390233,-2.01203427918534,340.566370923057));
#13384=CARTESIAN_POINT('Ctrl Pts',(104.071883035804,-1.86306400461667,340.617980681774));
#13385=CARTESIAN_POINT('Ctrl Pts',(104.064482169279,-1.71237226839279,340.6635423347));
#13386=CARTESIAN_POINT('Ctrl Pts',(104.057073175894,-1.56151505823562,340.709154018677));
#13387=CARTESIAN_POINT('Ctrl Pts',(104.049664182509,-1.4089329687871,340.74870422556));
#13388=CARTESIAN_POINT('Ctrl Pts',(104.042255189124,-1.25515553988395,340.782085707874));
#13389=CARTESIAN_POINT('Ctrl Pts',(104.034841631544,-1.10128337878004,340.815487754333));
#13390=CARTESIAN_POINT('Ctrl Pts',(104.027428073964,-0.946214777636154,
340.84271343954));
#13391=CARTESIAN_POINT('Ctrl Pts',(104.020014516384,-0.790486037222097,
340.863707222181));
#13392=CARTESIAN_POINT('Ctrl Pts',(104.012590404247,-0.634535588436436,
340.884730893315));
#13393=CARTESIAN_POINT('Ctrl Pts',(104.00516629211,-0.477923493913411,340.899504907259));
#13394=CARTESIAN_POINT('Ctrl Pts',(103.997742179974,-0.321188529049471,
340.90802576935));
#13395=CARTESIAN_POINT('Ctrl Pts',(103.993885054819,-0.239758404548028,
340.912452700263));
#13396=CARTESIAN_POINT('Ctrl Pts',(103.990027929664,-0.158295082796337,
340.915192625928));
#13397=CARTESIAN_POINT('Ctrl Pts',(103.986170804509,-0.0768736280428343,
340.916250586969));
#13398=CARTESIAN_POINT('Ctrl Pts',(103.978746827071,0.0798418060718854,
340.918286890843));
#13399=CARTESIAN_POINT('Ctrl Pts',(103.971322849633,0.236874618421677,340.914095118803));
#13400=CARTESIAN_POINT('Ctrl Pts',(103.963898872195,0.393688972301404,340.903637823884));
#13401=CARTESIAN_POINT('Ctrl Pts',(103.956483656168,0.550318261649561,340.893192870146));
#13402=CARTESIAN_POINT('Ctrl Pts',(103.94906844014,0.706729236947371,340.876497136512));
#13403=CARTESIAN_POINT('Ctrl Pts',(103.941653224113,0.862383886192894,340.853565118399));
#13404=CARTESIAN_POINT('Ctrl Pts',(103.934245142968,1.01788876531853,340.830655165358));
#13405=CARTESIAN_POINT('Ctrl Pts',(103.926837061824,1.1726384004148,340.801520927792));
#13406=CARTESIAN_POINT('Ctrl Pts',(103.91942898068,1.32609784140368,340.766228843666));
#13407=CARTESIAN_POINT('Ctrl Pts',(103.912026413506,1.47944305972823,340.730963028083));
#13408=CARTESIAN_POINT('Ctrl Pts',(103.904623846332,1.63149963391357,340.689548575441));
#13409=CARTESIAN_POINT('Ctrl Pts',(103.897221279158,1.78174088615125,340.642103329178));
#13410=CARTESIAN_POINT('Ctrl Pts',(103.889822609404,1.93190303702625,340.594683062629));
#13411=CARTESIAN_POINT('Ctrl Pts',(103.882423939649,2.08025141441344,340.541238438134));
#13412=CARTESIAN_POINT('Ctrl Pts',(103.875025269894,2.22627274091179,340.481937636053));
#13413=CARTESIAN_POINT('Ctrl Pts',(103.86762782069,2.37226997842538,340.422646616763));
#13414=CARTESIAN_POINT('Ctrl Pts',(103.860230371486,2.51594058150165,340.357501477549));
#13415=CARTESIAN_POINT('Ctrl Pts',(103.852832922282,2.65678945271268,340.286719244149));
#13416=CARTESIAN_POINT('Ctrl Pts',(103.845435793819,2.797632216962,340.215940079743));
#13417=CARTESIAN_POINT('Ctrl Pts',(103.838038665355,2.93565315913819,340.139524474711));
#13418=CARTESIAN_POINT('Ctrl Pts',(103.830641536892,3.07038032316165,340.057736176754));
#13419=CARTESIAN_POINT('Ctrl Pts',(103.823243269455,3.20512823180502,339.97593528544));
#13420=CARTESIAN_POINT('Ctrl Pts',(103.815845002019,3.33658103342749,339.8887602477));
#13421=CARTESIAN_POINT('Ctrl Pts',(103.808446734582,3.4642945149403,339.796518954018));
#13422=CARTESIAN_POINT('Ctrl Pts',(103.801045868056,3.59205286354241,339.704245254999));
#13423=CARTESIAN_POINT('Ctrl Pts',(103.79364500153,3.71606897417532,339.606901974782));
#13424=CARTESIAN_POINT('Ctrl Pts',(103.786244135005,3.83593068529685,339.50483810365));
#13425=CARTESIAN_POINT('Ctrl Pts',(103.77883514162,3.95592401603667,339.402662156629));
#13426=CARTESIAN_POINT('Ctrl Pts',(103.771426148235,4.07175355253006,339.295755508751));
#13427=CARTESIAN_POINT('Ctrl Pts',(103.76401715485,4.18304254369739,339.184505423598));
#13428=CARTESIAN_POINT('Ctrl Pts',(103.75660359727,4.29440009272229,339.073186804555));
#13429=CARTESIAN_POINT('Ctrl Pts',(103.74919003969,4.40121127016137,338.957519690084));
#13430=CARTESIAN_POINT('Ctrl Pts',(103.74177648211,4.50313914701812,338.837925010353));
#13431=CARTESIAN_POINT('Ctrl Pts',(103.734352369973,4.60521213686767,338.718160065701));
#13432=CARTESIAN_POINT('Ctrl Pts',(103.726928257836,4.70238771112937,338.594456680921));
#13433=CARTESIAN_POINT('Ctrl Pts',(103.7195041457,4.79437136878528,338.467266032578));
#13434=CARTESIAN_POINT('Ctrl Pts',(103.715647020545,4.84216058226133,338.401185369983));
#13435=CARTESIAN_POINT('Ctrl Pts',(103.71178989539,4.88854912197195,338.334163855773));
#13436=CARTESIAN_POINT('Ctrl Pts',(103.707932770235,4.93350060511098,338.266267340845));
#13437=CARTESIAN_POINT('Ctrl Pts',(103.700508792797,5.02002069021073,338.13558394979));
#13438=CARTESIAN_POINT('Ctrl Pts',(103.693084815359,5.10147520497793,338.001263299362));
#13439=CARTESIAN_POINT('Ctrl Pts',(103.685660837921,5.17754268747386,337.863735721376));
#13440=CARTESIAN_POINT('Ctrl Pts',(103.678245621894,5.2535203988957,337.726370446625));
#13441=CARTESIAN_POINT('Ctrl Pts',(103.670830405866,5.32412355388886,337.585806101144));
#13442=CARTESIAN_POINT('Ctrl Pts',(103.663415189838,5.38907319279343,337.442502955006));
#13443=CARTESIAN_POINT('Ctrl Pts',(103.656007108694,5.45396033748232,337.299337694435));
#13444=CARTESIAN_POINT('Ctrl Pts',(103.64859902755,5.51320464264368,337.153439217174));
#13445=CARTESIAN_POINT('Ctrl Pts',(103.641190946406,5.56657248519886,337.005293327553));
#13446=CARTESIAN_POINT('Ctrl Pts',(103.633788379232,5.61990060509416,336.857257705622));
#13447=CARTESIAN_POINT('Ctrl Pts',(103.626385812058,5.6673608456253,336.70697835172));
#13448=CARTESIAN_POINT('Ctrl Pts',(103.618983244884,5.70876728826917,336.554961932295));
#13449=CARTESIAN_POINT('Ctrl Pts',(103.611584575129,5.75015193060182,336.403025548852));
#13450=CARTESIAN_POINT('Ctrl Pts',(103.604185905375,5.78548902490515,336.249354280467));
#13451=CARTESIAN_POINT('Ctrl Pts',(103.59678723562,5.81464223377832,336.094470765101));
#13452=CARTESIAN_POINT('Ctrl Pts',(103.589389786416,5.84379063327737,335.939612800706));
#13453=CARTESIAN_POINT('Ctrl Pts',(103.581992337212,5.86675710304366,335.783543352644));
#13454=CARTESIAN_POINT('Ctrl Pts',(103.574594888008,5.88345621902356,335.626796203987));
#13455=CARTESIAN_POINT('Ctrl Pts',(103.567197759544,5.90015461095892,335.470055851613));
#13456=CARTESIAN_POINT('Ctrl Pts',(103.559800631081,5.91058614988309,335.312638228179));
#13457=CARTESIAN_POINT('Ctrl Pts',(103.552403502617,5.91471722435007,335.155082940637));
#13458=CARTESIAN_POINT('Ctrl Pts',(103.545005235181,5.91884893489939,334.997503393514));
#13459=CARTESIAN_POINT('Ctrl Pts',(103.537606967744,5.91667823958361,334.839786513182));
#13460=CARTESIAN_POINT('Ctrl Pts',(103.530208700308,5.90822366088908,334.682472465114));
#13461=CARTESIAN_POINT('Ctrl Pts',(103.522807833782,5.89976611201213,334.525103150967));
#13462=CARTESIAN_POINT('Ctrl Pts',(103.515406967256,5.885020304456,334.368137323286));
#13463=CARTESIAN_POINT('Ctrl Pts',(103.50800610073,5.86405666733463,334.212110436172));
#13464=CARTESIAN_POINT('Ctrl Pts',(103.500597107345,5.84307001013544,334.05591221662));
#13465=CARTESIAN_POINT('Ctrl Pts',(103.493188113961,5.81585193767445,333.900655366798));
#13466=CARTESIAN_POINT('Ctrl Pts',(103.485779120576,5.78252422653407,333.746866275274));
#13467=CARTESIAN_POINT('Ctrl Pts',(103.478365562996,5.74917598437415,333.592982444365));
#13468=CARTESIAN_POINT('Ctrl Pts',(103.470952005415,5.70971069710263,333.440568533923));
#13469=CARTESIAN_POINT('Ctrl Pts',(103.463538447835,5.66430000226331,333.290135664194));
#13470=CARTESIAN_POINT('Ctrl Pts',(103.456114335698,5.61882465698615,333.139488625735));
#13471=CARTESIAN_POINT('Ctrl Pts',(103.448690223562,5.56738712079512,332.990828612585));
#13472=CARTESIAN_POINT('Ctrl Pts',(103.441266111425,5.5102074262881,332.84464743446));
#13473=CARTESIAN_POINT('Ctrl Pts',(103.43740898627,5.48050027290022,332.768700427075));
#13474=CARTESIAN_POINT('Ctrl Pts',(103.433551861116,5.44924395237199,332.693422127347));
#13475=CARTESIAN_POINT('Ctrl Pts',(103.429694735961,5.41647415130372,332.618878766052));
#13476=CARTESIAN_POINT('Ctrl Pts',(103.422270758523,5.35340068232637,332.475401899155));
#13477=CARTESIAN_POINT('Ctrl Pts',(103.414846781085,5.2845272935753,332.334216448667));
#13478=CARTESIAN_POINT('Ctrl Pts',(103.407422803647,5.21004189875463,332.195825616029));
#13479=CARTESIAN_POINT('Ctrl Pts',(103.40000758762,5.13564440790693,332.057598105395));
#13480=CARTESIAN_POINT('Ctrl Pts',(103.392592371592,5.05564826935856,331.922158973189));
#13481=CARTESIAN_POINT('Ctrl Pts',(103.385177155564,4.97028957295405,331.789991881087));
#13482=CARTESIAN_POINT('Ctrl Pts',(103.37776907442,4.88501300825737,331.657951959496));
#13483=CARTESIAN_POINT('Ctrl Pts',(103.370360993276,4.79438435908125,331.529178121665));
#13484=CARTESIAN_POINT('Ctrl Pts',(103.362952912132,4.6986857217974,331.404129722824));
#13485=CARTESIAN_POINT('Ctrl Pts',(103.355550344958,4.60305831475735,331.27917439979));
#13486=CARTESIAN_POINT('Ctrl Pts',(103.348147777784,4.50236865941098,331.157939289584));
#13487=CARTESIAN_POINT('Ctrl Pts',(103.34074521061,4.39694221120499,331.040854921347));
#13488=CARTESIAN_POINT('Ctrl Pts',(103.333346540855,4.29157126956261,330.923832197517));
#13489=CARTESIAN_POINT('Ctrl Pts',(103.3259478711,4.18146875091419,330.810956140054));
#13490=CARTESIAN_POINT('Ctrl Pts',(103.318549201346,4.0670003726795,330.702624227377));
#13491=CARTESIAN_POINT('Ctrl Pts',(103.311151752142,3.95255087817319,330.594310186102));
#13492=CARTESIAN_POINT('Ctrl Pts',(103.303754302938,3.83373722430933,330.490539058099));
#13493=CARTESIAN_POINT('Ctrl Pts',(103.296356853734,3.71096205280173,330.391671538924));
#13494=CARTESIAN_POINT('Ctrl Pts',(103.28895972527,3.58819220461152,330.292808306472));
#13495=CARTESIAN_POINT('Ctrl Pts',(103.281562596807,3.46146147098186,330.198848494182));
#13496=CARTESIAN_POINT('Ctrl Pts',(103.274165468343,3.33120542982831,330.110112378921));
#13497=CARTESIAN_POINT('Ctrl Pts',(103.266767200907,3.20092933249567,330.021362600513));
#13498=CARTESIAN_POINT('Ctrl Pts',(103.25936893347,3.06712715529281,329.937838330774));
#13499=CARTESIAN_POINT('Ctrl Pts',(103.251970666033,2.93026315846882,329.85981630828));
#13500=CARTESIAN_POINT('Ctrl Pts',(103.244569799508,2.79335107988414,329.781766875831));
#13501=CARTESIAN_POINT('Ctrl Pts',(103.237168932982,2.65337536408568,329.709223723937));
#13502=CARTESIAN_POINT('Ctrl Pts',(103.229768066456,2.51082439908517,329.642417392195));
#13503=CARTESIAN_POINT('Ctrl Pts',(103.222359073071,2.36811689949608,329.575537700712));
#13504=CARTESIAN_POINT('Ctrl Pts',(103.214950079687,2.22282884144005,329.514407568442));
#13505=CARTESIAN_POINT('Ctrl Pts',(103.207541086302,2.0754687765893,329.459209449916));
#13506=CARTESIAN_POINT('Ctrl Pts',(103.200127528722,1.92801793285562,329.403977327444));
#13507=CARTESIAN_POINT('Ctrl Pts',(103.192713971141,1.77849289249599,329.354684617017));
#13508=CARTESIAN_POINT('Ctrl Pts',(103.185300413561,1.62741635035397,329.311463581456));
#13509=CARTESIAN_POINT('Ctrl Pts',(103.177876301424,1.47612472309606,329.268181012838));
#13510=CARTESIAN_POINT('Ctrl Pts',(103.170452189288,1.32327754419817,329.230987471168));
#13511=CARTESIAN_POINT('Ctrl Pts',(103.163028077151,1.16940745920663,329.199964072796));
#13512=CARTESIAN_POINT('Ctrl Pts',(103.159170951996,1.08946575514504,329.183846168321));
#13513=CARTESIAN_POINT('Ctrl Pts',(103.155313826842,1.0092480383871,329.169392867626));
#13514=CARTESIAN_POINT('Ctrl Pts',(103.151456701687,0.928829315873215,329.156610002364));
#13515=CARTESIAN_POINT('Ctrl Pts',(103.144032724249,0.774043884336897,329.132006262661));
#13516=CARTESIAN_POINT('Ctrl Pts',(103.136608746811,0.61804668435539,329.113519816133));
#13517=CARTESIAN_POINT('Ctrl Pts',(103.129184769373,0.46136255964295,329.101264953309));
#13518=CARTESIAN_POINT('Ctrl Pts',(103.121769553346,0.304863345772179,329.089024553067));
#13519=CARTESIAN_POINT('Ctrl Pts',(103.114354337318,0.147679189287689,329.083001126683));
#13520=CARTESIAN_POINT('Ctrl Pts',(103.106939121291,-0.00965542662716032,
329.083257878255));
#13521=CARTESIAN_POINT('Ctrl Pts',(103.099531040146,-0.166838655966651,
329.083514382781));
#13522=CARTESIAN_POINT('Ctrl Pts',(103.092122959002,-0.32417168580736,329.090039034659));
#13523=CARTESIAN_POINT('Ctrl Pts',(103.084714877858,-0.481115576003788,
329.102843196503));
#13524=CARTESIAN_POINT('Ctrl Pts',(103.077312310684,-0.637942649997047,
329.115637827976));
#13525=CARTESIAN_POINT('Ctrl Pts',(103.06990974351,-0.794380790686796,329.134702632675));
#13526=CARTESIAN_POINT('Ctrl Pts',(103.062507176336,-0.94989183431622,329.159996912193));
#13527=CARTESIAN_POINT('Ctrl Pts',(103.055108506582,-1.1053210020595,329.185277874383));
#13528=CARTESIAN_POINT('Ctrl Pts',(103.047709836827,-1.25982367740501,329.216781719728));
#13529=CARTESIAN_POINT('Ctrl Pts',(103.040311167072,-1.41286770159056,329.254416007027));
#13530=CARTESIAN_POINT('Ctrl Pts',(103.032913717868,-1.56588647826504,329.292044085838));
#13531=CARTESIAN_POINT('Ctrl Pts',(103.025516268664,-1.71744671929437,329.335800510401));
#13532=CARTESIAN_POINT('Ctrl Pts',(103.01811881946,-1.86702721555507,329.385541883772));
#13533=CARTESIAN_POINT('Ctrl Pts',(103.010721690997,-2.01660122626601,329.435281100444));
#13534=CARTESIAN_POINT('Ctrl Pts',(103.003324562533,-2.1641953087395,329.491004632191));
#13535=CARTESIAN_POINT('Ctrl Pts',(102.99592743407,-2.30930441912245,329.552519512442));
#13536=CARTESIAN_POINT('Ctrl Pts',(102.988529166633,-2.45443587268598,329.614043864449));
#13537=CARTESIAN_POINT('Ctrl Pts',(102.981130899197,-2.59708124867286,329.681361194825));
#13538=CARTESIAN_POINT('Ctrl Pts',(102.97373263176,-2.73675659384932,329.754230856345));
#13539=CARTESIAN_POINT('Ctrl Pts',(102.966331765235,-2.87648100844369,329.827126117744));
#13540=CARTESIAN_POINT('Ctrl Pts',(102.958930898709,-3.01323298413462,329.905577421394));
#13541=CARTESIAN_POINT('Ctrl Pts',(102.951530032183,-3.14655436048236,329.989298829602));
#13542=CARTESIAN_POINT('Ctrl Pts',(102.944121038798,-3.28002213644734,330.07311217192));
#13543=CARTESIAN_POINT('Ctrl Pts',(102.936712045414,-3.41005147366832,330.162206977305));
#13544=CARTESIAN_POINT('Ctrl Pts',(102.929303052029,-3.53621373574666,330.256254330424));
#13545=CARTESIAN_POINT('Ctrl Pts',(102.921889494449,-3.66245371813079,330.350359619958));
#13546=CARTESIAN_POINT('Ctrl Pts',(102.914475936868,-3.78482158902665,330.449423302345));
#13547=CARTESIAN_POINT('Ctrl Pts',(102.907062379288,-3.9029232656339,330.553077407344));
#13548=CARTESIAN_POINT('Ctrl Pts',(102.899638267151,-4.02119308159887,330.656879082938));
#13549=CARTESIAN_POINT('Ctrl Pts',(102.892214155015,-4.13518430314986,330.765283976961));
#13550=CARTESIAN_POINT('Ctrl Pts',(102.884790042878,-4.24454047274818,330.877888073123));
#13551=CARTESIAN_POINT('Ctrl Pts',(102.880932917723,-4.30135540560929,330.936390434598));
#13552=CARTESIAN_POINT('Ctrl Pts',(102.877075792568,-4.35691990394507,330.996025713659));
#13553=CARTESIAN_POINT('Ctrl Pts',(102.873218667413,-4.41118847323711,331.05673399121));
#13554=CARTESIAN_POINT('Ctrl Pts',(102.865865035668,-4.51465181909997,331.172474678664));
#13555=CARTESIAN_POINT('Ctrl Pts',(102.858511403922,-4.61372889142071,331.292482793505));
#13556=CARTESIAN_POINT('Ctrl Pts',(102.851157772177,-4.70804192368787,331.416388440791));
#13557=CARTESIAN_POINT('Ctrl Pts',(102.843611698532,-4.80482309410307,331.543536654321));
#13558=CARTESIAN_POINT('Ctrl Pts',(102.836065624887,-4.89658713161454,331.674788962405));
#13559=CARTESIAN_POINT('Ctrl Pts',(102.828519551243,-4.98296549190882,331.80970448564));
#13560=CARTESIAN_POINT('Ctrl Pts',(102.821183857563,-5.06693567581008,331.940858645763));
#13561=CARTESIAN_POINT('Ctrl Pts',(102.813848163883,-5.14581622420385,332.075474155608));
#13562=CARTESIAN_POINT('Ctrl Pts',(102.806512470203,-5.2193091077421,332.213112309342));
#13563=CARTESIAN_POINT('Ctrl Pts',(102.799181707702,-5.29275258811072,332.350657940362));
#13564=CARTESIAN_POINT('Ctrl Pts',(102.791850945201,-5.3608154310141,332.491221837879));
#13565=CARTESIAN_POINT('Ctrl Pts',(102.784520182699,-5.42324365377972,332.634337548542));
#13566=CARTESIAN_POINT('Ctrl Pts',(102.777192833119,-5.48564281236084,332.777386630024));
#13567=CARTESIAN_POINT('Ctrl Pts',(102.76986548354,-5.54241241982301,332.922984811724));
#13568=CARTESIAN_POINT('Ctrl Pts',(102.76253813396,-5.59334519502373,333.070642570231));
#13569=CARTESIAN_POINT('Ctrl Pts',(102.754830956522,-5.64691817275784,333.225954464735));
#13570=CARTESIAN_POINT('Ctrl Pts',(102.747123779084,-5.69403286319964,333.383544751446));
#13571=CARTESIAN_POINT('Ctrl Pts',(102.739416601646,-5.73450626313315,333.542821740285));
#13572=CARTESIAN_POINT('Ctrl Pts',(102.73208993929,-5.77298142970359,333.694234981734));
#13573=CARTESIAN_POINT('Ctrl Pts',(102.724763276934,-5.80545524539736,333.84717197329));
#13574=CARTESIAN_POINT('Ctrl Pts',(102.717436614578,-5.83182233017694,334.001111181487));
#13575=CARTESIAN_POINT('Ctrl Pts',(102.710109070923,-5.85819258656002,334.155068906489));
#13576=CARTESIAN_POINT('Ctrl Pts',(102.702781527269,-5.87845459279923,334.310028711433));
#13577=CARTESIAN_POINT('Ctrl Pts',(102.695453983615,-5.89255456859799,334.46546167715));
#13578=CARTESIAN_POINT('Ctrl Pts',(102.688122269657,-5.90666256907455,334.620983103975));
#13579=CARTESIAN_POINT('Ctrl Pts',(102.680790555699,-5.91460151443724,334.77697784916));
#13580=CARTESIAN_POINT('Ctrl Pts',(102.673458841741,-5.91636967316463,334.932914584612));
#13581=CARTESIAN_POINT('Ctrl Pts',(102.672323229395,-5.91664354403461,334.957067693005));
#13582=CARTESIAN_POINT('Ctrl Pts',(102.67118761705,-5.91676947294849,334.981219413314));
#13583=CARTESIAN_POINT('Ctrl Pts',(102.670052004704,-5.91674756512981,335.005367777056));
#13584=CARTESIAN_POINT('',(100.920052004704,-5.92200910417624,334.999274282758));
#13585=CARTESIAN_POINT('Ctrl Pts',(102.67005103823,-5.91455807452654,335.005386334829));
#13586=CARTESIAN_POINT('Ctrl Pts',(102.645027569866,-5.91924007014113,335.537308585578));
#13587=CARTESIAN_POINT('Ctrl Pts',(102.52725809008,-5.60948765469108,338.03536527471));
#13588=CARTESIAN_POINT('Ctrl Pts',(102.316742598864,-2.08285686558825,341.679395945644));
#13589=CARTESIAN_POINT('Ctrl Pts',(102.038504564592,4.48969318508649,340.366123183922));
#13590=CARTESIAN_POINT('Ctrl Pts',(101.760266530317,6.94211806756556,334.128438380165));
#13591=CARTESIAN_POINT('Ctrl Pts',(101.482028496044,3.02386366494078,328.690572810701));
#13592=CARTESIAN_POINT('Ctrl Pts',(101.203790461769,-3.66934579084986,329.042775445864));
#13593=CARTESIAN_POINT('Ctrl Pts',(101.016464964656,-5.90853212608389,332.960493776982));
#13594=CARTESIAN_POINT('Ctrl Pts',(100.921885478968,-5.92645748560412,334.960501290448));
#13595=CARTESIAN_POINT('Ctrl Pts',(100.920052004704,-5.92639050991422,334.999273745835));
#13596=CARTESIAN_POINT('',(99.1700520270116,-5.9141281310151,334.995021507455));
#13597=CARTESIAN_POINT('Ctrl Pts',(100.920052004704,-5.9167499555727,334.999274927244));
#13598=CARTESIAN_POINT('Ctrl Pts',(100.912653210428,-5.91676909816112,335.155482574443));
#13599=CARTESIAN_POINT('Ctrl Pts',(100.905254416151,-5.91059793288327,335.311933625634));
#13600=CARTESIAN_POINT('Ctrl Pts',(100.897855621875,-5.89820461626513,335.468094933928));
#13601=CARTESIAN_POINT('Ctrl Pts',(100.890465537159,-5.88582588855612,335.62407241547));
#13602=CARTESIAN_POINT('Ctrl Pts',(100.883075452442,-5.86723961667127,335.779760461813));
#13603=CARTESIAN_POINT('Ctrl Pts',(100.875685367726,-5.8424659210364,335.934624268906));
#13604=CARTESIAN_POINT('Ctrl Pts',(100.868302342465,-5.8177158907311,336.089340140743));
#13605=CARTESIAN_POINT('Ctrl Pts',(100.860919317204,-5.78679026122925,336.243232971833));
#13606=CARTESIAN_POINT('Ctrl Pts',(100.853536291943,-5.74976106211383,336.395771575545));
#13607=CARTESIAN_POINT('Ctrl Pts',(100.84615868182,-5.71275902235735,336.548198298612));
#13608=CARTESIAN_POINT('Ctrl Pts',(100.838781071697,-5.66966241415348,336.699272407962));
#13609=CARTESIAN_POINT('Ctrl Pts',(100.831403461574,-5.62059457665737,336.848471576019));
#13610=CARTESIAN_POINT('Ctrl Pts',(100.823733083726,-5.56957956671361,337.003591455566));
#13611=CARTESIAN_POINT('Ctrl Pts',(100.816062705878,-5.51210974251225,337.156684117268));
#13612=CARTESIAN_POINT('Ctrl Pts',(100.80839232803,-5.44838152063113,337.30717779292));
#13613=CARTESIAN_POINT('Ctrl Pts',(100.801019583112,-5.3871261387845,337.451831877021));
#13614=CARTESIAN_POINT('Ctrl Pts',(100.793646838194,-5.32008909750129,337.594084513008));
#13615=CARTESIAN_POINT('Ctrl Pts',(100.786274093277,-5.24749442809488,337.733447052645));
#13616=CARTESIAN_POINT('Ctrl Pts',(100.778901455742,-5.17490081601893,337.872807562487));
#13617=CARTESIAN_POINT('Ctrl Pts',(100.771528818207,-5.09674991022246,338.009277726004));
#13618=CARTESIAN_POINT('Ctrl Pts',(100.764156180672,-5.01331204470294,338.142392862921));
#13619=CARTESIAN_POINT('Ctrl Pts',(100.756782169677,-4.92985863541142,338.275532798067));
#13620=CARTESIAN_POINT('Ctrl Pts',(100.749408158682,-4.84111650543503,338.405316143782));
#13621=CARTESIAN_POINT('Ctrl Pts',(100.742034147687,-4.74739960743119,338.531306773683));
#13622=CARTESIAN_POINT('Ctrl Pts',(100.734657281808,-4.65364642647555,338.657346181469));
#13623=CARTESIAN_POINT('Ctrl Pts',(100.727280415929,-4.5549148676611,338.779589648939));
#13624=CARTESIAN_POINT('Ctrl Pts',(100.719903550049,-4.4515593534164,338.897633882949));
#13625=CARTESIAN_POINT('Ctrl Pts',(100.712518519967,-4.34808945246633,339.015808760119));
#13626=CARTESIAN_POINT('Ctrl Pts',(100.705133489885,-4.23998562652681,339.129774842121));
#13627=CARTESIAN_POINT('Ctrl Pts',(100.697748459803,-4.12763980697507,339.239165034105));
#13628=CARTESIAN_POINT('Ctrl Pts',(100.690358595546,-4.01522044684805,339.348626831935));
#13629=CARTESIAN_POINT('Ctrl Pts',(100.682968731289,-3.89855384004281,339.453506522037));
#13630=CARTESIAN_POINT('Ctrl Pts',(100.675578867032,-3.77806473386628,339.553477509466));
#13631=CARTESIAN_POINT('Ctrl Pts',(100.668178963507,-3.65741194100149,339.653584309339));
#13632=CARTESIAN_POINT('Ctrl Pts',(100.660779059982,-3.53292657951394,339.748768866886));
#13633=CARTESIAN_POINT('Ctrl Pts',(100.653379156457,-3.40506255255605,339.838747728047));
#13634=CARTESIAN_POINT('Ctrl Pts',(100.651357568712,-3.3701312390514,339.863329151633));
#13635=CARTESIAN_POINT('Ctrl Pts',(100.649335980967,-3.33494790616683,339.887522321181));
#13636=CARTESIAN_POINT('Ctrl Pts',(100.647314393222,-3.2995221135164,339.911322060802));
#13637=CARTESIAN_POINT('Ctrl Pts',(100.639890415784,-3.16942620944326,339.998723030857));
#13638=CARTESIAN_POINT('Ctrl Pts',(100.632466438346,-3.03565890746535,340.081083118453));
#13639=CARTESIAN_POINT('Ctrl Pts',(100.625042460908,-2.89864835787401,340.158077961789));
#13640=CARTESIAN_POINT('Ctrl Pts',(100.61762724488,-2.76179950134534,340.234981939626));
#13641=CARTESIAN_POINT('Ctrl Pts',(100.610212028852,-2.62171533813551,340.306533095682));
#13642=CARTESIAN_POINT('Ctrl Pts',(100.602796812825,-2.47885424324229,340.372449367212));
#13643=CARTESIAN_POINT('Ctrl Pts',(100.595388731681,-2.33613060857546,340.438302214438));
#13644=CARTESIAN_POINT('Ctrl Pts',(100.587980650537,-2.1906356981925,340.49853081573));
#13645=CARTESIAN_POINT('Ctrl Pts',(100.580572569393,-2.04285372704659,340.552898271389));
#13646=CARTESIAN_POINT('Ctrl Pts',(100.573170002219,-1.89518175272074,340.607225260357));
#13647=CARTESIAN_POINT('Ctrl Pts',(100.565767435045,-1.74522645592163,340.655699661874));
#13648=CARTESIAN_POINT('Ctrl Pts',(100.558364867871,-1.59349323552573,340.698132138766));
#13649=CARTESIAN_POINT('Ctrl Pts',(100.550966198116,-1.44183990200765,340.740542275144));
#13650=CARTESIAN_POINT('Ctrl Pts',(100.543567528361,-1.28841086764603,340.776916721881));
#13651=CARTESIAN_POINT('Ctrl Pts',(100.536168858607,-1.13372783741781,340.807115613897));
#13652=CARTESIAN_POINT('Ctrl Pts',(100.528771409403,-0.979070325085853,
340.837309524033));
#13653=CARTESIAN_POINT('Ctrl Pts',(100.521373960199,-0.823159593397856,
340.861329829943));
#13654=CARTESIAN_POINT('Ctrl Pts',(100.513976510995,-0.666528836142006,
340.879087503439));
#13655=CARTESIAN_POINT('Ctrl Pts',(100.506579382531,-0.509904870122723,
340.896844406993));
#13656=CARTESIAN_POINT('Ctrl Pts',(100.499182254068,-0.352561311445007,
340.908339175994));
#13657=CARTESIAN_POINT('Ctrl Pts',(100.491785125605,-0.195037527677288,
340.913534554334));
#13658=CARTESIAN_POINT('Ctrl Pts',(100.484386858168,-0.0374894891794162,
340.918730732632));
#13659=CARTESIAN_POINT('Ctrl Pts',(100.476988590731,0.120238456631527,340.917625576671));
#13660=CARTESIAN_POINT('Ctrl Pts',(100.469590323295,0.277606031478055,340.910233959311));
#13661=CARTESIAN_POINT('Ctrl Pts',(100.462189456769,0.435028891208541,340.902839745197));
#13662=CARTESIAN_POINT('Ctrl Pts',(100.454788590243,0.592090755344619,340.889154690065));
#13663=CARTESIAN_POINT('Ctrl Pts',(100.447387723718,0.748255706205567,340.869245604047));
#13664=CARTESIAN_POINT('Ctrl Pts',(100.439978730333,0.904592141112852,340.84931465595));
#13665=CARTESIAN_POINT('Ctrl Pts',(100.432569736948,1.06002932541838,340.823146075169));
#13666=CARTESIAN_POINT('Ctrl Pts',(100.425160743564,1.21404005987996,340.790858079379));
#13667=CARTESIAN_POINT('Ctrl Pts',(100.417747185983,1.36814567026627,340.75855019307));
#13668=CARTESIAN_POINT('Ctrl Pts',(100.410333628403,1.52082271872443,340.720115470881));
#13669=CARTESIAN_POINT('Ctrl Pts',(100.402920070823,1.67155893713738,340.675722093459));
#13670=CARTESIAN_POINT('Ctrl Pts',(100.395495958686,1.8225097561533,340.631265513937));
#13671=CARTESIAN_POINT('Ctrl Pts',(100.38807184655,1.97151387404858,340.580833455787));
#13672=CARTESIAN_POINT('Ctrl Pts',(100.380647734413,2.11807800585394,340.524642624063));
#13673=CARTESIAN_POINT('Ctrl Pts',(100.376790609258,2.19422397309841,340.495449224702));
#13674=CARTESIAN_POINT('Ctrl Pts',(100.372933484103,2.26971171367343,340.464702175955));
#13675=CARTESIAN_POINT('Ctrl Pts',(100.369076358949,2.34447475722508,340.432436716174));
#13676=CARTESIAN_POINT('Ctrl Pts',(100.361652381511,2.4883744561581,340.370333974928));
#13677=CARTESIAN_POINT('Ctrl Pts',(100.354228404073,2.63002197355981,340.302415966113));
#13678=CARTESIAN_POINT('Ctrl Pts',(100.346804426635,2.76891284998212,340.228867199662));
#13679=CARTESIAN_POINT('Ctrl Pts',(100.339389210607,2.9076398142731,340.155405231822));
#13680=CARTESIAN_POINT('Ctrl Pts',(100.331973994579,3.04361628661856,340.07632590656));
#13681=CARTESIAN_POINT('Ctrl Pts',(100.324558778552,3.17635702142493,339.991862040857));
#13682=CARTESIAN_POINT('Ctrl Pts',(100.317150697408,3.30897003376444,339.907479445859));
#13683=CARTESIAN_POINT('Ctrl Pts',(100.309742616264,3.43835319401689,339.817722823796));
#13684=CARTESIAN_POINT('Ctrl Pts',(100.302334535119,3.56404525167383,339.72287116133));
#13685=CARTESIAN_POINT('Ctrl Pts',(100.294931967945,3.68964375443676,339.628090098688));
#13686=CARTESIAN_POINT('Ctrl Pts',(100.287529400771,3.81155632835938,339.528221770575));
#13687=CARTESIAN_POINT('Ctrl Pts',(100.280126833597,3.92935025544174,339.423588716479));
#13688=CARTESIAN_POINT('Ctrl Pts',(100.272728163843,4.04708216453596,339.319010751229));
#13689=CARTESIAN_POINT('Ctrl Pts',(100.265329494088,4.16069946706159,339.209673303264));
#13690=CARTESIAN_POINT('Ctrl Pts',(100.257930824333,4.26980222298958,339.095939396409));
#13691=CARTESIAN_POINT('Ctrl Pts',(100.250533375129,4.37888698035122,338.982224252116));
#13692=CARTESIAN_POINT('Ctrl Pts',(100.243135925925,4.4834584111145,338.864114357442));
#13693=CARTESIAN_POINT('Ctrl Pts',(100.235738476721,4.58315310782257,338.742009908158));
#13694=CARTESIAN_POINT('Ctrl Pts',(100.228341348258,4.68284348194232,338.619910753111));
#13695=CARTESIAN_POINT('Ctrl Pts',(100.220944219794,4.77765730639749,338.493817676917));
#13696=CARTESIAN_POINT('Ctrl Pts',(100.213547091331,4.86727136899175,338.364164083854));
#13697=CARTESIAN_POINT('Ctrl Pts',(100.206148823894,4.95689922991459,338.234490527375));
#13698=CARTESIAN_POINT('Ctrl Pts',(100.198750556457,5.04132552259523,338.101255669459));
#13699=CARTESIAN_POINT('Ctrl Pts',(100.191352289021,5.12027037836295,337.964921890195));
#13700=CARTESIAN_POINT('Ctrl Pts',(100.183951422495,5.19924296828892,337.828540215441));
#13701=CARTESIAN_POINT('Ctrl Pts',(100.176550555969,5.27273010036275,337.68905777454));
#13702=CARTESIAN_POINT('Ctrl Pts',(100.169149689443,5.34049794084267,337.546961386899));
#13703=CARTESIAN_POINT('Ctrl Pts',(100.161740696059,5.40834019689005,337.404708963841));
#13704=CARTESIAN_POINT('Ctrl Pts',(100.154331702674,5.47045045844053,337.259837198837));
#13705=CARTESIAN_POINT('Ctrl Pts',(100.146922709289,5.52664283949753,337.112853399347));
#13706=CARTESIAN_POINT('Ctrl Pts',(100.139509151709,5.58286983699978,336.965779052765));
#13707=CARTESIAN_POINT('Ctrl Pts',(100.132095594128,5.63317157067045,336.816590431933));
#13708=CARTESIAN_POINT('Ctrl Pts',(100.124682036548,5.67741224953052,336.665809326238));
#13709=CARTESIAN_POINT('Ctrl Pts',(100.117257924411,5.72171591309616,336.514813556035));
#13710=CARTESIAN_POINT('Ctrl Pts',(100.109833812275,5.75994119752516,336.362221133977));
#13711=CARTESIAN_POINT('Ctrl Pts',(100.102409700138,5.79200338991732,336.208564145458));
#13712=CARTESIAN_POINT('Ctrl Pts',(100.098552574983,5.80866098970979,336.128733153592));
#13713=CARTESIAN_POINT('Ctrl Pts',(100.094695449829,5.82365588836928,336.048614909744));
#13714=CARTESIAN_POINT('Ctrl Pts',(100.090838324674,5.8369817476534,335.968284379747));
#13715=CARTESIAN_POINT('Ctrl Pts',(100.083414347236,5.86263061169119,335.813668696206));
#13716=CARTESIAN_POINT('Ctrl Pts',(100.075990369798,5.88217050851072,335.657799945201));
#13717=CARTESIAN_POINT('Ctrl Pts',(100.06856639236,5.89548360449685,335.501202186357));
#13718=CARTESIAN_POINT('Ctrl Pts',(100.061151176332,5.90878098902664,335.34478923643));
#13719=CARTESIAN_POINT('Ctrl Pts',(100.053735960305,5.91586616884547,335.187649359434));
#13720=CARTESIAN_POINT('Ctrl Pts',(100.046320744277,5.91667233048297,335.030316599369));
#13721=CARTESIAN_POINT('Ctrl Pts',(100.038912663133,5.91747771643579,334.873135224092));
#13722=CARTESIAN_POINT('Ctrl Pts',(100.031504581989,5.91201611008612,334.715761705935));
#13723=CARTESIAN_POINT('Ctrl Pts',(100.024096500845,5.90027250815382,334.558734895982));
#13724=CARTESIAN_POINT('Ctrl Pts',(100.016693933671,5.88853764719892,334.401824963951));
#13725=CARTESIAN_POINT('Ctrl Pts',(100.009291366497,5.87053012858272,334.245261596863));
#13726=CARTESIAN_POINT('Ctrl Pts',(100.001888799323,5.84628701410339,334.089583221142));
#13727=CARTESIAN_POINT('Ctrl Pts',(99.9944901295682,5.82205666351787,333.933986809405));
#13728=CARTESIAN_POINT('Ctrl Pts',(99.9870914598135,5.79159731266814,333.779274828917));
#13729=CARTESIAN_POINT('Ctrl Pts',(99.9796927900588,5.75499780553456,333.625980050803));
#13730=CARTESIAN_POINT('Ctrl Pts',(99.9722953408548,5.71840433618311,333.472710561566));
#13731=CARTESIAN_POINT('Ctrl Pts',(99.9648978916508,5.67567280748164,333.320858173352));
#13732=CARTESIAN_POINT('Ctrl Pts',(99.9575004424468,5.62694309196391,333.170945052138));
#13733=CARTESIAN_POINT('Ctrl Pts',(99.9501033139833,5.57821548928169,333.021038430895));
#13734=CARTESIAN_POINT('Ctrl Pts',(99.9427061855198,5.52349033226132,332.873071264399));
#13735=CARTESIAN_POINT('Ctrl Pts',(99.9353090570564,5.46295717114055,332.727549888604));
#13736=CARTESIAN_POINT('Ctrl Pts',(99.9279107896197,5.40241468942382,332.582006106149));
#13737=CARTESIAN_POINT('Ctrl Pts',(99.9205125221831,5.33606256631044,332.438909208845));
#13738=CARTESIAN_POINT('Ctrl Pts',(99.9131142547465,5.2641381740847,332.298744764624));
#13739=CARTESIAN_POINT('Ctrl Pts',(99.9057133882207,5.19218851406397,332.158531079162));
#13740=CARTESIAN_POINT('Ctrl Pts',(99.898312521695,5.11466285763911,332.02125222975));
#13741=CARTESIAN_POINT('Ctrl Pts',(99.8909116551692,5.03184404078075,331.887368298086));
#13742=CARTESIAN_POINT('Ctrl Pts',(99.8835026617844,4.94893428094351,331.753337349065));
#13743=CARTESIAN_POINT('Ctrl Pts',(99.8760936683997,4.86071994945993,331.62270908028));
#13744=CARTESIAN_POINT('Ctrl Pts',(99.8686846750149,4.76752705841442,331.495914340404));
#13745=CARTESIAN_POINT('Ctrl Pts',(99.8612711174347,4.67427675733347,331.369041490595));
#13746=CARTESIAN_POINT('Ctrl Pts',(99.8538575598544,4.57604201767905,331.246007166438));
#13747=CARTESIAN_POINT('Ctrl Pts',(99.8464440022742,4.47318813898736,331.127207927642));
#13748=CARTESIAN_POINT('Ctrl Pts',(99.8390198901375,4.37018782896944,331.00823955638));
#13749=CARTESIAN_POINT('Ctrl Pts',(99.8315957780008,4.26255550061586,330.893518583876));
#13750=CARTESIAN_POINT('Ctrl Pts',(99.8241716658641,4.15069275287367,330.783404188953));
#13751=CARTESIAN_POINT('Ctrl Pts',(99.8203145407094,4.0925755517534,330.726195327512));
#13752=CARTESIAN_POINT('Ctrl Pts',(99.8164574155547,4.03331701132481,330.670229218396));
#13753=CARTESIAN_POINT('Ctrl Pts',(99.8126002904001,3.97297674196854,330.615551759882));
#13754=CARTESIAN_POINT('Ctrl Pts',(99.8051763129621,3.85683718716056,330.510311664708));
#13755=CARTESIAN_POINT('Ctrl Pts',(99.7977523355241,3.73633798849539,330.409530623692));
#13756=CARTESIAN_POINT('Ctrl Pts',(99.7903283580861,3.6118560723602,330.313591324366));
#13757=CARTESIAN_POINT('Ctrl Pts',(99.7829131420584,3.48752106361527,330.217765247849));
#13758=CARTESIAN_POINT('Ctrl Pts',(99.7754979260309,3.35921298596517,330.126769764857));
#13759=CARTESIAN_POINT('Ctrl Pts',(99.7680827100032,3.22734477179831,330.040950062114));
#13760=CARTESIAN_POINT('Ctrl Pts',(99.7606746288591,3.09560344056336,329.955212934657));
#13761=CARTESIAN_POINT('Ctrl Pts',(99.7532665477151,2.96030910314582,329.874641875189));
#13762=CARTESIAN_POINT('Ctrl Pts',(99.745858466571,2.82190677178258,329.799541103531));
#13763=CARTESIAN_POINT('Ctrl Pts',(99.738455899397,2.68360745580221,329.724496230748));
#13764=CARTESIAN_POINT('Ctrl Pts',(99.731053332223,2.54220507869098,329.65491371579));
#13765=CARTESIAN_POINT('Ctrl Pts',(99.723650765049,2.39817247098011,329.591053766034));
#13766=CARTESIAN_POINT('Ctrl Pts',(99.7162520952942,2.25421569580709,329.527227438262));
#13767=CARTESIAN_POINT('Ctrl Pts',(99.7088534255395,2.10763178827678,329.469117826199));
#13768=CARTESIAN_POINT('Ctrl Pts',(99.7014547557847,1.95891684556952,329.416938532074));
#13769=CARTESIAN_POINT('Ctrl Pts',(99.6940573065807,1.8102264362106,329.364767845911));
#13770=CARTESIAN_POINT('Ctrl Pts',(99.6866598573768,1.65940604121787,329.318525659483));
#13771=CARTESIAN_POINT('Ctrl Pts',(99.6792624081728,1.50697045415601,329.278376924963));
#13772=CARTESIAN_POINT('Ctrl Pts',(99.6718652797094,1.35454147643524,329.238229931221));
#13773=CARTESIAN_POINT('Ctrl Pts',(99.6644681512459,1.20049780679511,329.204175959125));
#13774=CARTESIAN_POINT('Ctrl Pts',(99.6570710227824,1.04536781045199,329.176329619272));
#13775=CARTESIAN_POINT('Ctrl Pts',(99.6496727553458,0.890213927962546,329.148478991778));
#13776=CARTESIAN_POINT('Ctrl Pts',(99.6422744879093,0.73397375308156,329.126837965635));
#13777=CARTESIAN_POINT('Ctrl Pts',(99.6348762204727,0.5771840660067,329.111469698095));
#13778=CARTESIAN_POINT('Ctrl Pts',(99.6274753539469,0.420339297065263,329.096096031522));
#13779=CARTESIAN_POINT('Ctrl Pts',(99.6200744874212,0.262945002766155,329.086999547471));
#13780=CARTESIAN_POINT('Ctrl Pts',(99.6126736208954,0.105541134396792,329.084191379748));
#13781=CARTESIAN_POINT('Ctrl Pts',(99.6052646275107,-0.0520355784683301,
329.081380128388));
#13782=CARTESIAN_POINT('Ctrl Pts',(99.597855634126,-0.20962151302473,329.084870990014));
#13783=CARTESIAN_POINT('Ctrl Pts',(99.5904466407412,-0.366677935584943,
329.09462297105));
#13784=CARTESIAN_POINT('Ctrl Pts',(99.583033083161,-0.523831110318572,329.104380959642));
#13785=CARTESIAN_POINT('Ctrl Pts',(99.5756195255808,-0.680453752658934,
329.120407715454));
#13786=CARTESIAN_POINT('Ctrl Pts',(99.5682059680006,-0.836014702547161,
329.142610651525));
#13787=CARTESIAN_POINT('Ctrl Pts',(99.5607818558639,-0.991797121927017,
329.164845197541));
#13788=CARTESIAN_POINT('Ctrl Pts',(99.5533577437272,-1.14651446398342,329.193273417778));
#13789=CARTESIAN_POINT('Ctrl Pts',(99.5459336315905,-1.29964735934819,329.227751971386));
#13790=CARTESIAN_POINT('Ctrl Pts',(99.5420765064357,-1.37920606372499,329.245664968115));
#13791=CARTESIAN_POINT('Ctrl Pts',(99.5382193812809,-1.45833735534825,329.26521026601));
#13792=CARTESIAN_POINT('Ctrl Pts',(99.5343622561261,-1.53697037878076,329.286362575622));
#13793=CARTESIAN_POINT('Ctrl Pts',(99.5269382786881,-1.68831879720438,329.327075350815));
#13794=CARTESIAN_POINT('Ctrl Pts',(99.5195143012501,-1.83827675530462,329.373867293602));
#13795=CARTESIAN_POINT('Ctrl Pts',(99.5120903238121,-1.9863184664741,329.426628532724));
#13796=CARTESIAN_POINT('Ctrl Pts',(99.5046751077845,-2.13418546615065,329.479327505646));
#13797=CARTESIAN_POINT('Ctrl Pts',(99.4972598917568,-2.28014037223469,329.537981628309));
#13798=CARTESIAN_POINT('Ctrl Pts',(99.4898446757292,-2.42366944843697,329.602430457399));
#13799=CARTESIAN_POINT('Ctrl Pts',(99.4824365945851,-2.56706042168449,329.66681727415));
#13800=CARTESIAN_POINT('Ctrl Pts',(99.475028513441,-2.70802987366323,329.736987545419));
#13801=CARTESIAN_POINT('Ctrl Pts',(99.4676204322969,-2.84608115778066,329.812731681721));
#13802=CARTESIAN_POINT('Ctrl Pts',(99.4602178651229,-2.98402968780591,329.888419440278));
#13803=CARTESIAN_POINT('Ctrl Pts',(99.4528152979489,-3.11906404903283,329.969672624391));
#13804=CARTESIAN_POINT('Ctrl Pts',(99.4454127307749,-3.25070955179678,330.05623443392));
#13805=CARTESIAN_POINT('Ctrl Pts',(99.4380140610203,-3.3822857437771,330.142750669033));
#13806=CARTESIAN_POINT('Ctrl Pts',(99.4306153912657,-3.51047631961996,330.234569758688));
#13807=CARTESIAN_POINT('Ctrl Pts',(99.4232167215111,-3.63483319000509,330.331390116605));
#13808=CARTESIAN_POINT('Ctrl Pts',(99.4158192723071,-3.75916954537005,330.42819450217));
#13809=CARTESIAN_POINT('Ctrl Pts',(99.4084218231031,-3.879673156275,330.529998289478));
#13810=CARTESIAN_POINT('Ctrl Pts',(99.4010243738991,-3.99592672658031,330.636457842727));
#13811=CARTESIAN_POINT('Ctrl Pts',(99.3936272454357,-4.11217525633365,330.742912780075));
#13812=CARTESIAN_POINT('Ctrl Pts',(99.3862301169722,-4.22417383664596,330.854022829934));
#13813=CARTESIAN_POINT('Ctrl Pts',(99.3788329885087,-4.33154016028266,330.969405701096));
#13814=CARTESIAN_POINT('Ctrl Pts',(99.3714347210721,-4.43892301565267,331.084806338339));
#13815=CARTESIAN_POINT('Ctrl Pts',(99.3640364536355,-4.5416719399151,331.204480833627));
#13816=CARTESIAN_POINT('Ctrl Pts',(99.3566381861989,-4.63944334022348,331.328011975053));
#13817=CARTESIAN_POINT('Ctrl Pts',(99.3492373196732,-4.73724908865262,331.451586514268));
#13818=CARTESIAN_POINT('Ctrl Pts',(99.3418364531475,-4.83007360008329,331.579020104727));
#13819=CARTESIAN_POINT('Ctrl Pts',(99.3344355866218,-4.91761531323803,331.709864715014));
#13820=CARTESIAN_POINT('Ctrl Pts',(99.327026593237,-5.00525315556376,331.840853005194));
#13821=CARTESIAN_POINT('Ctrl Pts',(99.3196175998523,-5.0875964070157,331.975259485043));
#13822=CARTESIAN_POINT('Ctrl Pts',(99.3122086064675,-5.16438800025667,332.112608937933));
#13823=CARTESIAN_POINT('Ctrl Pts',(99.3047950488872,-5.24122689976794,332.250043002824));
#13824=CARTESIAN_POINT('Ctrl Pts',(99.297381491307,-5.31250715766586,332.390423321351));
#13825=CARTESIAN_POINT('Ctrl Pts',(99.2899679337267,-5.37801919111498,332.533253125572));
#13826=CARTESIAN_POINT('Ctrl Pts',(99.28254382159,-5.44362449293725,332.676286274168));
#13827=CARTESIAN_POINT('Ctrl Pts',(99.2751197094533,-5.50344502751617,332.821775529035));
#13828=CARTESIAN_POINT('Ctrl Pts',(99.2676955973166,-5.5573202726657,332.969206571431));
#13829=CARTESIAN_POINT('Ctrl Pts',(99.2638384721618,-5.58531063157485,333.04580293363));
#13830=CARTESIAN_POINT('Ctrl Pts',(99.259981347007,-5.61169705604384,333.122923207148));
#13831=CARTESIAN_POINT('Ctrl Pts',(99.2561242218521,-5.63646246856781,333.200494122564));
#13832=CARTESIAN_POINT('Ctrl Pts',(99.2471743973967,-5.69392653461697,333.380484671991));
#13833=CARTESIAN_POINT('Ctrl Pts',(99.2382245729412,-5.74280101829535,333.563341817107));
#13834=CARTESIAN_POINT('Ctrl Pts',(99.2292747484858,-5.78283892385022,333.748319312563));
#13835=CARTESIAN_POINT('Ctrl Pts',(99.2203760436108,-5.82264814101625,333.932240254115));
#13836=CARTESIAN_POINT('Ctrl Pts',(99.2114773387359,-5.85372137608482,334.118257381203));
#13837=CARTESIAN_POINT('Ctrl Pts',(99.2025786338609,-5.87586259412093,334.305615857388));
#13838=CARTESIAN_POINT('Ctrl Pts',(99.1937730964491,-5.89777199852301,334.49101273195));
#13839=CARTESIAN_POINT('Ctrl Pts',(99.1849675590373,-5.91093537759809,334.677722982322));
#13840=CARTESIAN_POINT('Ctrl Pts',(99.1761620216254,-5.91520955858939,334.864994665021));
#13841=CARTESIAN_POINT('Ctrl Pts',(99.1741253679381,-5.91619814407475,334.90830917784));
#13842=CARTESIAN_POINT('Ctrl Pts',(99.1720887142508,-5.91671139333383,334.951653638754));
#13843=CARTESIAN_POINT('Ctrl Pts',(99.1700520605635,-5.91674790303204,334.995018587954));
#13844=CARTESIAN_POINT('',(97.4200520047035,-5.90851871549448,335.003050241221));
#13845=CARTESIAN_POINT('Ctrl Pts',(99.1700520047035,-5.91238628844001,334.995023448582));
#13846=CARTESIAN_POINT('Ctrl Pts',(99.1059967323284,-5.90156737437933,336.357909306957));
#13847=CARTESIAN_POINT('Ctrl Pts',(98.9491954485287,-4.75485099692124,339.710562044037));
#13848=CARTESIAN_POINT('Ctrl Pts',(98.6996481533043,0.824642780502851,341.947847667141));
#13849=CARTESIAN_POINT('Ctrl Pts',(98.4214101190303,6.28885485565189,338.066419332996));
#13850=CARTESIAN_POINT('Ctrl Pts',(98.1431720847566,5.9818776531124,331.37098323724));
#13851=CARTESIAN_POINT('Ctrl Pts',(97.8649340504824,0.185419620684727,328.005842260465));
#13852=CARTESIAN_POINT('Ctrl Pts',(97.6238940237982,-4.98351069473949,330.650937683327));
#13853=CARTESIAN_POINT('Ctrl Pts',(97.4756000085385,-5.90300490085091,333.819225757616));
#13854=CARTESIAN_POINT('Ctrl Pts',(97.4200520047035,-5.90851871549448,335.003050241221));
#13855=CARTESIAN_POINT('',(95.6700520047035,-5.92356759530611,335.003691307709));
#13856=CARTESIAN_POINT('Ctrl Pts',(97.4200520047035,-5.90851871549448,335.003050241221));
#13857=CARTESIAN_POINT('Ctrl Pts',(97.3828539971138,-5.91221106994108,335.795804419332));
#13858=CARTESIAN_POINT('Ctrl Pts',(97.2529099780996,-5.39419567492929,338.560510449033));
#13859=CARTESIAN_POINT('Ctrl Pts',(97.0302199476606,-1.19160955147132,341.894395520859));
#13860=CARTESIAN_POINT('Ctrl Pts',(96.7519819133865,5.15279597612825,339.733002910377));
#13861=CARTESIAN_POINT('Ctrl Pts',(96.4737438791129,6.76855669157607,333.228203388051));
#13862=CARTESIAN_POINT('Ctrl Pts',(96.1955058448389,2.17291283490253,328.349355464833));
#13863=CARTESIAN_POINT('Ctrl Pts',(95.927608553369,-4.17187446274379,329.528202769892));
#13864=CARTESIAN_POINT('Ctrl Pts',(95.752457273324,-5.91083243971606,333.258866916678));
#13865=CARTESIAN_POINT('Ctrl Pts',(95.6700520047035,-5.92356759530611,335.003691307709));
#13866=CARTESIAN_POINT('',(93.9200520047036,-5.91881622079639,334.9949747712));
#13867=CARTESIAN_POINT('Ctrl Pts',(95.6700520047035,-5.92356759530611,335.003691307709));
#13868=CARTESIAN_POINT('Ctrl Pts',(95.6597112618994,-5.92516568449061,335.222643087955));
#13869=CARTESIAN_POINT('Ctrl Pts',(95.5566245076704,-5.8146635492223,337.403741509423));
#13870=CARTESIAN_POINT('Ctrl Pts',(95.3607917420169,-3.10883504916976,341.267995497622));
#13871=CARTESIAN_POINT('Ctrl Pts',(95.0825537077432,3.58852210574754,341.006257738209));
#13872=CARTESIAN_POINT('Ctrl Pts',(94.8043156734692,6.99274549072358,335.232665904654));
#13873=CARTESIAN_POINT('Ctrl Pts',(94.5260776391951,3.97982955161444,329.245560004544));
#13874=CARTESIAN_POINT('Ctrl Pts',(94.2478396049213,-2.68531722482238,328.539218752868));
#13875=CARTESIAN_POINT('Ctrl Pts',(94.0458310600907,-5.73526615944503,332.330987701425));
#13876=CARTESIAN_POINT('Ctrl Pts',(93.9365685266848,-5.92317375626255,334.644710114703));
#13877=CARTESIAN_POINT('Ctrl Pts',(93.9200520047036,-5.92000683156533,334.994973760341));
#13878=CARTESIAN_POINT('',(92.1700520270473,-5.91150425643539,334.998948922259));
#13879=CARTESIAN_POINT('Ctrl Pts',(93.9200520047036,-5.91674786747094,334.994976527286));
#13880=CARTESIAN_POINT('Ctrl Pts',(93.9127497712506,-5.91687927201086,335.149747454818));
#13881=CARTESIAN_POINT('Ctrl Pts',(93.9054475377976,-5.91093376253086,335.304730384447));
#13882=CARTESIAN_POINT('Ctrl Pts',(93.8981453043445,-5.89888816629507,335.459400657427));
#13883=CARTESIAN_POINT('Ctrl Pts',(93.8908494566086,-5.88685310379126,335.613935673075));
#13884=CARTESIAN_POINT('Ctrl Pts',(93.8835536088727,-5.8687285990787,335.76815819435));
#13885=CARTESIAN_POINT('Ctrl Pts',(93.8762577611368,-5.84454352770003,335.921543007851));
#13886=CARTESIAN_POINT('Ctrl Pts',(93.8689665925407,-5.82037396724416,336.074829449099));
#13887=CARTESIAN_POINT('Ctrl Pts',(93.8616754239446,-5.79015163599576,336.227278872607));
#13888=CARTESIAN_POINT('Ctrl Pts',(93.8543842553485,-5.75395726397602,336.378370910473));
#13889=CARTESIAN_POINT('Ctrl Pts',(93.8470952608465,-5.71777368446038,336.529417895438));
#13890=CARTESIAN_POINT('Ctrl Pts',(93.8398062663444,-5.6756216927509,336.679107924966));
#13891=CARTESIAN_POINT('Ctrl Pts',(93.8325172718423,-5.6276331552403,336.826930658931));
#13892=CARTESIAN_POINT('Ctrl Pts',(93.8252291497028,-5.57965036110126,336.974735701151));
#13893=CARTESIAN_POINT('Ctrl Pts',(93.8179410275632,-5.52583252932446,337.120673525813));
#13894=CARTESIAN_POINT('Ctrl Pts',(93.8106529054237,-5.46636134326529,337.264249153109));
#13895=CARTESIAN_POINT('Ctrl Pts',(93.8033641179255,-5.40688472786907,337.407837887937));
#13896=CARTESIAN_POINT('Ctrl Pts',(93.7960753304273,-5.34175387893055,337.549063640338));
#13897=CARTESIAN_POINT('Ctrl Pts',(93.788786542929,-5.27119842506811,337.687451902092));
#13898=CARTESIAN_POINT('Ctrl Pts',(93.7814955519873,-5.20062164187481,337.825881999437));
#13899=CARTESIAN_POINT('Ctrl Pts',(93.7742045610455,-5.12461716627325,337.961472556544));
#13900=CARTESIAN_POINT('Ctrl Pts',(93.7669135701037,-5.04346016314264,338.093774417325));
#13901=CARTESIAN_POINT('Ctrl Pts',(93.7596149443138,-4.96221817548822,338.226214819577));
#13902=CARTESIAN_POINT('Ctrl Pts',(93.7523163185239,-4.87581309023246,338.355359321746));
#13903=CARTESIAN_POINT('Ctrl Pts',(93.745017692734,-4.78456321040497,338.480788049873));
#13904=CARTESIAN_POINT('Ctrl Pts',(93.7377147095408,-4.69325885285226,338.606291661078));
#13905=CARTESIAN_POINT('Ctrl Pts',(93.7304117263475,-4.59710417957538,338.728074779704));
#13906=CARTESIAN_POINT('Ctrl Pts',(93.7231087431543,-4.49645666286742,338.845751947468));
#13907=CARTESIAN_POINT('Ctrl Pts',(93.7157956129763,-4.39566930346896,338.963592619433));
#13908=CARTESIAN_POINT('Ctrl Pts',(93.7084824827983,-4.29037689992064,339.07731567077));
#13909=CARTESIAN_POINT('Ctrl Pts',(93.7011693526203,-4.18097292138371,339.186573299628));
#13910=CARTESIAN_POINT('Ctrl Pts',(93.6979007472047,-4.13207478501374,339.235406024971));
#13911=CARTESIAN_POINT('Ctrl Pts',(93.6946321417891,-4.08235573426027,339.283347262807));
#13912=CARTESIAN_POINT('Ctrl Pts',(93.6913635363735,-4.03185287865414,339.330368682617));
#13913=CARTESIAN_POINT('Ctrl Pts',(93.6839395589355,-3.91714583607711,339.437168346505));
#13914=CARTESIAN_POINT('Ctrl Pts',(93.6765155814975,-3.7980193007917,339.539568266908));
#13915=CARTESIAN_POINT('Ctrl Pts',(93.6690916040594,-3.67484499424399,339.637180698526));
#13916=CARTESIAN_POINT('Ctrl Pts',(93.6616763880318,-3.55181605191058,339.734677932788));
#13917=CARTESIAN_POINT('Ctrl Pts',(93.6542611720041,-3.42474913662316,339.827398695052));
#13918=CARTESIAN_POINT('Ctrl Pts',(93.6468459559765,-3.29405247922026,339.914992250924));
#13919=CARTESIAN_POINT('Ctrl Pts',(93.6394378748324,-3.16348157748305,340.002501524718));
#13920=CARTESIAN_POINT('Ctrl Pts',(93.6320297936882,-3.02928819453711,340.084893207155));
#13921=CARTESIAN_POINT('Ctrl Pts',(93.6246217125441,-2.89191319164979,340.161857093572));
#13922=CARTESIAN_POINT('Ctrl Pts',(93.6172191453701,-2.75464043948608,340.238763694363));
#13923=CARTESIAN_POINT('Ctrl Pts',(93.6098165781961,-2.61419110688851,340.310250361747));
#13924=CARTESIAN_POINT('Ctrl Pts',(93.602414011022,-2.47103446553667,340.376050523631));
#13925=CARTESIAN_POINT('Ctrl Pts',(93.5950153412673,-2.32795319553085,340.441816042017));
#13926=CARTESIAN_POINT('Ctrl Pts',(93.5876166715125,-2.18216779376351,340.501900862));
#13927=CARTESIAN_POINT('Ctrl Pts',(93.5802180017578,-2.0341714261272,340.556084698025));
#13928=CARTESIAN_POINT('Ctrl Pts',(93.5728205525538,-1.88619947329581,340.610259595399));
#13929=CARTESIAN_POINT('Ctrl Pts',(93.5654231033498,-1.73601762860874,340.658535312671));
#13930=CARTESIAN_POINT('Ctrl Pts',(93.5580256541458,-1.58413840995274,340.700739957287));
#13931=CARTESIAN_POINT('Ctrl Pts',(93.5506285256823,-1.4322657765151,340.742942771984));
#13932=CARTESIAN_POINT('Ctrl Pts',(93.5432313972188,-1.278696275026,340.779074937492));
#13933=CARTESIAN_POINT('Ctrl Pts',(93.5358342687553,-1.12395667395598,340.809014714869));
#13934=CARTESIAN_POINT('Ctrl Pts',(93.5284360013186,-0.969193246849669,
340.838959102226));
#13935=CARTESIAN_POINT('Ctrl Pts',(93.521037733882,-0.813259727865903,340.862709132061));
#13936=CARTESIAN_POINT('Ctrl Pts',(93.5136394664454,-0.656691994880478,
340.880194400388));
#13937=CARTESIAN_POINT('Ctrl Pts',(93.5062385999196,-0.500069258004175,
340.897685811475));
#13938=CARTESIAN_POINT('Ctrl Pts',(93.4988377333938,-0.342812234191548,
340.908908037715));
#13939=CARTESIAN_POINT('Ctrl Pts',(93.491436866868,-0.185460675013545,340.913842650978));
#13940=CARTESIAN_POINT('Ctrl Pts',(93.4840278734832,-0.0279363287802752,
340.918782682918));
#13941=CARTESIAN_POINT('Ctrl Pts',(93.4766188800984,0.129682386879827,340.917421301719));
#13942=CARTESIAN_POINT('Ctrl Pts',(93.4692098867137,0.286856233585559,340.909792218323));
#13943=CARTESIAN_POINT('Ctrl Pts',(93.4617963291334,0.444126904802365,340.902158435149));
#13944=CARTESIAN_POINT('Ctrl Pts',(93.4543827715531,0.60095179009131,340.888249288879));
#13945=CARTESIAN_POINT('Ctrl Pts',(93.4469692139729,0.756798526924307,340.868150181458));
#13946=CARTESIAN_POINT('Ctrl Pts',(93.4395451018362,0.912867140118635,340.848022459278));
#13947=CARTESIAN_POINT('Ctrl Pts',(93.4321209896994,1.06795445665763,340.821687237847));
#13948=CARTESIAN_POINT('Ctrl Pts',(93.4246968775627,1.22153921788592,340.789280827673));
#13949=CARTESIAN_POINT('Ctrl Pts',(93.4208397524083,1.3013326847631,340.772444392886));
#13950=CARTESIAN_POINT('Ctrl Pts',(93.4169826272538,1.38072083211056,340.753970031105));
#13951=CARTESIAN_POINT('Ctrl Pts',(93.4131255020994,1.45963246927007,340.733882072135));
#13952=CARTESIAN_POINT('Ctrl Pts',(93.4057015246614,1.61151714773126,340.695217899158));
#13953=CARTESIAN_POINT('Ctrl Pts',(93.3982775472234,1.76209362912566,340.650456326819));
#13954=CARTESIAN_POINT('Ctrl Pts',(93.3908535697854,1.910834690356,340.599700112384));
#13955=CARTESIAN_POINT('Ctrl Pts',(93.3834383537578,2.05940021475512,340.549003797918));
#13956=CARTESIAN_POINT('Ctrl Pts',(93.3760231377301,2.20613428081304,340.492327042776));
#13957=CARTESIAN_POINT('Ctrl Pts',(93.3686079217025,2.35052103136587,340.429823334475));
#13958=CARTESIAN_POINT('Ctrl Pts',(93.3611998405584,2.49476885371421,340.367379766927));
#13959=CARTESIAN_POINT('Ctrl Pts',(93.3537917594143,2.63667351675123,340.299120555318));
#13960=CARTESIAN_POINT('Ctrl Pts',(93.3463836782702,2.77573558743026,340.22524855975));
#13961=CARTESIAN_POINT('Ctrl Pts',(93.3389811110962,2.9146941516701,340.151431548458));
#13962=CARTESIAN_POINT('Ctrl Pts',(93.3315785439222,3.05081400822313,340.072010245948));
#13963=CARTESIAN_POINT('Ctrl Pts',(93.3241759767482,3.18361704109762,339.98723501533));
#13964=CARTESIAN_POINT('Ctrl Pts',(93.3167773069935,3.31635015375534,339.902504418501));
#13965=CARTESIAN_POINT('Ctrl Pts',(93.3093786372387,3.44576960679308,339.81242570772));
#13966=CARTESIAN_POINT('Ctrl Pts',(93.301979967484,3.57142327702471,339.717294387552));
#13967=CARTESIAN_POINT('Ctrl Pts',(93.29458251828,3.69705621830304,339.622178761097));
#13968=CARTESIAN_POINT('Ctrl Pts',(93.287185069076,3.81892431246661,339.522012404587));
#13969=CARTESIAN_POINT('Ctrl Pts',(93.2797876198721,3.93660565856321,339.417133284322));
#13970=CARTESIAN_POINT('Ctrl Pts',(93.2723904914086,4.05428190220172,339.312258711434));
#13971=CARTESIAN_POINT('Ctrl Pts',(93.2649933629451,4.16777148009504,339.20267202939));
#13972=CARTESIAN_POINT('Ctrl Pts',(93.2575962344817,4.27668695472454,339.088750329109));
#13973=CARTESIAN_POINT('Ctrl Pts',(93.2501979670451,4.38561919961824,338.97481108773));
#13974=CARTESIAN_POINT('Ctrl Pts',(93.2427996996084,4.48997568097655,338.856535768842));
#13975=CARTESIAN_POINT('Ctrl Pts',(93.2354014321718,4.58940720031757,338.734336903946));
#13976=CARTESIAN_POINT('Ctrl Pts',(93.2280005656461,4.68887365099706,338.612095109303));
#13977=CARTESIAN_POINT('Ctrl Pts',(93.2205996991203,4.78341145944938,338.485927313598));
#13978=CARTESIAN_POINT('Ctrl Pts',(93.2131988325946,4.87271303851913,338.356277432923));
#13979=CARTESIAN_POINT('Ctrl Pts',(93.2057898392098,4.96211267926027,338.226485184283));
#13980=CARTESIAN_POINT('Ctrl Pts',(93.1983808458251,5.04626439597001,338.093203522154));
#13981=CARTESIAN_POINT('Ctrl Pts',(93.1909718524403,5.12490472406927,337.956904146521));
#13982=CARTESIAN_POINT('Ctrl Pts',(93.1835582948601,5.20359349732318,337.820520805771));
#13983=CARTESIAN_POINT('Ctrl Pts',(93.1761447372798,5.27676394352619,337.681116376867));
#13984=CARTESIAN_POINT('Ctrl Pts',(93.1687311796996,5.34419978708432,337.539184750708));
#13985=CARTESIAN_POINT('Ctrl Pts',(93.1613070675629,5.41173163791164,337.397051058895));
#13986=CARTESIAN_POINT('Ctrl Pts',(93.1538829554262,5.47351243426087,337.252383326344));
#13987=CARTESIAN_POINT('Ctrl Pts',(93.1464588432895,5.52937471957837,337.105693656016));
#13988=CARTESIAN_POINT('Ctrl Pts',(93.1426017181348,5.55839742585336,337.029482466458));
#13989=CARTESIAN_POINT('Ctrl Pts',(93.1387445929801,5.58582342272072,336.952725742459));
#13990=CARTESIAN_POINT('Ctrl Pts',(93.1348874678255,5.61163464428278,336.875496516015));
#13991=CARTESIAN_POINT('Ctrl Pts',(93.1274634903875,5.66131463101879,336.726850047032));
#13992=CARTESIAN_POINT('Ctrl Pts',(93.1200395129495,5.7051592440521,336.576004016209));
#13993=CARTESIAN_POINT('Ctrl Pts',(93.1126155355115,5.74296958348887,336.423457384547));
#13994=CARTESIAN_POINT('Ctrl Pts',(93.1052003194839,5.78073530103625,336.271090780862));
#13995=CARTESIAN_POINT('Ctrl Pts',(93.0977851034563,5.81248083123473,336.117027929962));
#13996=CARTESIAN_POINT('Ctrl Pts',(93.0903698874287,5.83805608510027,335.961785688043));
#13997=CARTESIAN_POINT('Ctrl Pts',(93.0829618062846,5.86360673058536,335.806692819427));
#13998=CARTESIAN_POINT('Ctrl Pts',(93.0755537251405,5.88299885895413,335.650423184761));
#13999=CARTESIAN_POINT('Ctrl Pts',(93.0681456439964,5.89613278771588,335.493506547192));
#14000=CARTESIAN_POINT('Ctrl Pts',(93.0607430768224,5.90925694065456,335.336706705543));
#14001=CARTESIAN_POINT('Ctrl Pts',(93.0533405096484,5.9161321379307,335.179261190196));
#14002=CARTESIAN_POINT('Ctrl Pts',(93.0459379424744,5.91671017922907,335.021707544934));
#14003=CARTESIAN_POINT('Ctrl Pts',(93.0385392727197,5.91728791619122,334.86423685098));
#14004=CARTESIAN_POINT('Ctrl Pts',(93.0311406029651,5.9115750986757,334.706658512759));
#14005=CARTESIAN_POINT('Ctrl Pts',(93.0237419332104,5.89957555297738,334.549512644782));
#14006=CARTESIAN_POINT('Ctrl Pts',(93.0163444840064,5.88757798683141,334.392392700992));
#14007=CARTESIAN_POINT('Ctrl Pts',(93.0089470348025,5.86929577922842,334.235705457616));
#14008=CARTESIAN_POINT('Ctrl Pts',(93.0015495855985,5.84478481842733,334.079988593124));
#14009=CARTESIAN_POINT('Ctrl Pts',(92.9941524571351,5.8202749203788,333.924278480245));
#14010=CARTESIAN_POINT('Ctrl Pts',(92.9867553286716,5.78953686414773,333.769539031264));
#14011=CARTESIAN_POINT('Ctrl Pts',(92.9793582002081,5.75267808885966,333.616300116191));
#14012=CARTESIAN_POINT('Ctrl Pts',(92.9719599327716,5.7158136382404,333.46303760615));
#14013=CARTESIAN_POINT('Ctrl Pts',(92.964561665335,5.6728266793312,333.311276452942));
#14014=CARTESIAN_POINT('Ctrl Pts',(92.9571633978984,5.62387514733678,333.161533549485));
#14015=CARTESIAN_POINT('Ctrl Pts',(92.9497625313727,5.57490641815424,333.011738039772));
#14016=CARTESIAN_POINT('Ctrl Pts',(92.9423616648469,5.51996905980628,332.863962546006));
#14017=CARTESIAN_POINT('Ctrl Pts',(92.9349607983212,5.45926991774558,332.718705953259));
#14018=CARTESIAN_POINT('Ctrl Pts',(92.9275518049365,5.39850412222383,332.573289854885));
#14019=CARTESIAN_POINT('Ctrl Pts',(92.9201428115517,5.33196405163685,332.430398525928));
#14020=CARTESIAN_POINT('Ctrl Pts',(92.912733818167,5.25990379276315,332.2905087833));
#14021=CARTESIAN_POINT('Ctrl Pts',(92.9053202605868,5.18779914228446,332.150532863765));
#14022=CARTESIAN_POINT('Ctrl Pts',(92.8979067030065,5.11016771091606,332.013562539026));
#14023=CARTESIAN_POINT('Ctrl Pts',(92.8904931454263,5.02730778291849,331.880046952548));
#14024=CARTESIAN_POINT('Ctrl Pts',(92.8830690332896,4.94432988864364,331.746341282189));
#14025=CARTESIAN_POINT('Ctrl Pts',(92.875644921153,4.85610883987707,331.616100481387));
#14026=CARTESIAN_POINT('Ctrl Pts',(92.8682208090163,4.76298465457447,331.489742496228));
#14027=CARTESIAN_POINT('Ctrl Pts',(92.8643636838614,4.71460289106556,331.424094435678));
#14028=CARTESIAN_POINT('Ctrl Pts',(92.8605065587065,4.66489830492699,331.359493862144));
#14029=CARTESIAN_POINT('Ctrl Pts',(92.8566494335516,4.61392253382932,331.29599548943));
#14030=CARTESIAN_POINT('Ctrl Pts',(92.8492254561136,4.51580723828781,331.173777395008));
#14031=CARTESIAN_POINT('Ctrl Pts',(92.8418014786756,4.41268442872467,331.055276081702));
#14032=CARTESIAN_POINT('Ctrl Pts',(92.8343775012376,4.30486605594624,330.940928825105));
#14033=CARTESIAN_POINT('Ctrl Pts',(92.8269622852099,4.19717492507007,330.826716515476));
#14034=CARTESIAN_POINT('Ctrl Pts',(92.8195470691823,4.08479951490953,330.716648773124));
#14035=CARTESIAN_POINT('Ctrl Pts',(92.8121318531547,3.9680932391058,330.611131511624));
#14036=CARTESIAN_POINT('Ctrl Pts',(92.8047237720106,3.85149925749286,330.505715778301));
#14037=CARTESIAN_POINT('Ctrl Pts',(92.7973156908665,3.73058298121668,330.404842057776));
#14038=CARTESIAN_POINT('Ctrl Pts',(92.7899076097224,3.60573595549293,330.308880860417));
#14039=CARTESIAN_POINT('Ctrl Pts',(92.7825050425484,3.48098185569005,330.212991088729));
#14040=CARTESIAN_POINT('Ctrl Pts',(92.7751024753743,3.35230312662593,330.122006786087));
#14041=CARTESIAN_POINT('Ctrl Pts',(92.7676999082003,3.2201257163797,330.03625938095));
#14042=CARTESIAN_POINT('Ctrl Pts',(92.7603012384455,3.08801789696211,329.950557121446));
#14043=CARTESIAN_POINT('Ctrl Pts',(92.7529025686907,2.95241537720475,329.870086470917));
#14044=CARTESIAN_POINT('Ctrl Pts',(92.7455038989359,2.81377442154918,329.795136498703));
#14045=CARTESIAN_POINT('Ctrl Pts',(92.7381064497319,2.67515633734705,329.720198890907));
#14046=CARTESIAN_POINT('Ctrl Pts',(92.7307090005279,2.53350114004959,329.650780331211));
#14047=CARTESIAN_POINT('Ctrl Pts',(92.723311551324,2.38929121929656,329.58712479066));
#14048=CARTESIAN_POINT('Ctrl Pts',(92.7159144228605,2.24508755123427,329.523472010101));
#14049=CARTESIAN_POINT('Ctrl Pts',(92.708517294397,2.09832972138873,329.465581902562));
#14050=CARTESIAN_POINT('Ctrl Pts',(92.7011201659335,1.94952145022995,329.413650863257));
#14051=CARTESIAN_POINT('Ctrl Pts',(92.6937218984969,1.80069026631196,329.361711827867));
#14052=CARTESIAN_POINT('Ctrl Pts',(92.6863236310603,1.64980836483906,329.315733810647));
#14053=CARTESIAN_POINT('Ctrl Pts',(92.6789253636237,1.49739587989629,329.27586372093));
#14054=CARTESIAN_POINT('Ctrl Pts',(92.6715244970979,1.34492985084431,329.235979624431));
#14055=CARTESIAN_POINT('Ctrl Pts',(92.6641236305721,1.19093252857694,329.20220782207));
#14056=CARTESIAN_POINT('Ctrl Pts',(92.6567227640463,1.03593537213602,329.174644348432));
#14057=CARTESIAN_POINT('Ctrl Pts',(92.6493137706616,0.880768013999356,329.147050607464));
#14058=CARTESIAN_POINT('Ctrl Pts',(92.6419047772768,0.724598996762802,329.12567887519));
#14059=CARTESIAN_POINT('Ctrl Pts',(92.634495783892,0.567966786876173,329.110573517608));
#14060=CARTESIAN_POINT('Ctrl Pts',(92.6270822263118,0.411238086145321,329.095458854604));
#14061=CARTESIAN_POINT('Ctrl Pts',(92.6196686687315,0.254045995933292,329.086618279364));
#14062=CARTESIAN_POINT('Ctrl Pts',(92.6122551111513,0.096929629291864,329.084044015591));
#14063=CARTESIAN_POINT('Ctrl Pts',(92.6048309990146,-0.0604104212611402,
329.081466086882));
#14064=CARTESIAN_POINT('Ctrl Pts',(92.5974068868779,-0.217674160831285,
329.085172278375));
#14065=CARTESIAN_POINT('Ctrl Pts',(92.5899827747412,-0.374326126412815,
329.095102836324));
#14066=CARTESIAN_POINT('Ctrl Pts',(92.5861256495867,-0.455713129441094,
329.10026216099));
#14067=CARTESIAN_POINT('Ctrl Pts',(92.5822685244321,-0.536935133518491,
329.107100730755));
#14068=CARTESIAN_POINT('Ctrl Pts',(92.5784113992776,-0.617918184534345,
329.115604731179));
#14069=CARTESIAN_POINT('Ctrl Pts',(92.5709874218396,-0.773789803814569,
329.131972752633));
#14070=CARTESIAN_POINT('Ctrl Pts',(92.5635634444016,-0.929245755728457,
329.15456306299));
#14071=CARTESIAN_POINT('Ctrl Pts',(92.5561394669636,-1.08374951142005,329.183349971075));
#14072=CARTESIAN_POINT('Ctrl Pts',(92.5487242509359,-1.23807092943315,329.212102906276));
#14073=CARTESIAN_POINT('Ctrl Pts',(92.5413090349083,-1.39144202470665,329.247037815032));
#14074=CARTESIAN_POINT('Ctrl Pts',(92.5338938188807,-1.54333020345631,329.288077167398));
#14075=CARTESIAN_POINT('Ctrl Pts',(92.5264857377366,-1.69507223616481,329.329077031905));
#14076=CARTESIAN_POINT('Ctrl Pts',(92.5190776565926,-1.845333835068,329.376169549952));
#14077=CARTESIAN_POINT('Ctrl Pts',(92.5116695754485,-1.99359154250904,329.429225967234));
#14078=CARTESIAN_POINT('Ctrl Pts',(92.5042670082745,-2.14173889903071,329.482242893656));
#14079=CARTESIAN_POINT('Ctrl Pts',(92.4968644411006,-2.28788498406668,329.541214755328));
#14080=CARTESIAN_POINT('Ctrl Pts',(92.4894618739266,-2.43152058740869,329.60596271838));
#14081=CARTESIAN_POINT('Ctrl Pts',(92.4820632041719,-2.57508056723278,329.670676591912));
#14082=CARTESIAN_POINT('Ctrl Pts',(92.4746645344172,-2.71613235833852,329.741160357322));
#14083=CARTESIAN_POINT('Ctrl Pts',(92.4672658646625,-2.85418596528124,329.817186764112));
#14084=CARTESIAN_POINT('Ctrl Pts',(92.4598684154585,-2.99221679766649,329.893200628907));
#14085=CARTESIAN_POINT('Ctrl Pts',(92.4524709662546,-3.12725010092552,329.974755140508));
#14086=CARTESIAN_POINT('Ctrl Pts',(92.4450735170506,-3.25881966589009,330.061576673906));
#14087=CARTESIAN_POINT('Ctrl Pts',(92.4376763885871,-3.39038352622762,330.148394442874));
#14088=CARTESIAN_POINT('Ctrl Pts',(92.4302792601237,-3.51848363537998,330.240478574009));
#14089=CARTESIAN_POINT('Ctrl Pts',(92.4228821316602,-3.64268224837314,330.33751175874));
#14090=CARTESIAN_POINT('Ctrl Pts',(92.4154838642236,-3.76689998485228,330.43455988416));
#14091=CARTESIAN_POINT('Ctrl Pts',(92.408085596787,-3.8872147349197,330.536558350696));
#14092=CARTESIAN_POINT('Ctrl Pts',(92.4006873293505,-4.00322148498267,330.64314926757));
#14093=CARTESIAN_POINT('Ctrl Pts',(92.3932864628247,-4.11926898943731,330.749777630955));
#14094=CARTESIAN_POINT('Ctrl Pts',(92.385885596299,-4.23100520597538,330.861001404555));
#14095=CARTESIAN_POINT('Ctrl Pts',(92.3784847297732,-4.33806177408423,330.976425642948));
#14096=CARTESIAN_POINT('Ctrl Pts',(92.3710757363884,-4.44523590053988,331.091976628189));
#14097=CARTESIAN_POINT('Ctrl Pts',(92.3636667430036,-4.54771986235856,331.211737015859));
#14098=CARTESIAN_POINT('Ctrl Pts',(92.3562577496189,-4.64518495613238,331.335278007021));
#14099=CARTESIAN_POINT('Ctrl Pts',(92.3488441920386,-4.74271009176625,331.458895103696));
#14100=CARTESIAN_POINT('Ctrl Pts',(92.3414306344583,-4.83520997978545,331.586297143367));
#14101=CARTESIAN_POINT('Ctrl Pts',(92.334017076878,-4.92239941443725,331.717026566168));
#14102=CARTESIAN_POINT('Ctrl Pts',(92.3265929647413,-5.00971297921125,331.847942106235));
#14103=CARTESIAN_POINT('Ctrl Pts',(92.3191688526046,-5.0917007969904,331.982194172792));
#14104=CARTESIAN_POINT('Ctrl Pts',(92.3117447404679,-5.16812334621587,332.119300147395));
#14105=CARTESIAN_POINT('Ctrl Pts',(92.3078876153132,-5.20782793736116,332.190532221179));
#14106=CARTESIAN_POINT('Ctrl Pts',(92.3040304901585,-5.24603112507699,332.262534279703));
#14107=CARTESIAN_POINT('Ctrl Pts',(92.3001733650038,-5.28270450540837,332.335236657593));
#14108=CARTESIAN_POINT('Ctrl Pts',(92.2922446478177,-5.3580904079244,332.484683867605));
#14109=CARTESIAN_POINT('Ctrl Pts',(92.2843159306316,-5.42721247029743,332.637494118537));
#14110=CARTESIAN_POINT('Ctrl Pts',(92.2763872134455,-5.48977933379852,332.793134931923));
#14111=CARTESIAN_POINT('Ctrl Pts',(92.2684733496026,-5.5522289870276,332.948484174004));
#14112=CARTESIAN_POINT('Ctrl Pts',(92.2605594857598,-5.60814781624935,333.106653132832));
#14113=CARTESIAN_POINT('Ctrl Pts',(92.2526456219169,-5.65729082478846,333.267085955316));
#14114=CARTESIAN_POINT('Ctrl Pts',(92.2447527932948,-5.70630321015079,333.427092343897));
#14115=CARTESIAN_POINT('Ctrl Pts',(92.2368599646728,-5.74857561356557,333.58935031139));
#14116=CARTESIAN_POINT('Ctrl Pts',(92.2289671360507,-5.78391172835668,333.75328604681));
#14117=CARTESIAN_POINT('Ctrl Pts',(92.22108714372,-5.81919037519964,333.916955169718));
#14118=CARTESIAN_POINT('Ctrl Pts',(92.2132071513893,-5.84755515751885,334.08229633424));
#14119=CARTESIAN_POINT('Ctrl Pts',(92.2053271590587,-5.86885928070626,334.248720221377));
#14120=CARTESIAN_POINT('Ctrl Pts',(92.1974651758119,-5.89011471504646,334.414763760206));
#14121=CARTESIAN_POINT('Ctrl Pts',(92.1896031925652,-5.90434163731046,334.581884794039));
#14122=CARTESIAN_POINT('Ctrl Pts',(92.1817412093184,-5.91144417937927,334.749483979389));
#14123=CARTESIAN_POINT('Ctrl Pts',(92.1778448241734,-5.91496418680491,334.832545842486));
#14124=CARTESIAN_POINT('Ctrl Pts',(92.1739484390285,-5.91673510119079,334.915724957293));
#14125=CARTESIAN_POINT('Ctrl Pts',(92.1700520538834,-5.91674990637331,334.998947416805));
#14126=CARTESIAN_POINT('',(90.4200520047035,-5.91614342231082,335.00545103649));
#14127=CARTESIAN_POINT('Ctrl Pts',(92.1700520047035,-5.90713672806163,334.9989501757));
#14128=CARTESIAN_POINT('Ctrl Pts',(92.1206797800456,-5.90547239974453,336.051773050695));
#14129=CARTESIAN_POINT('Ctrl Pts',(91.9785615439628,-5.13393945780749,339.08460722529));
#14130=CARTESIAN_POINT('Ctrl Pts',(91.7436972964561,-0.279901569715299,
341.991014091852));
#14131=CARTESIAN_POINT('Ctrl Pts',(91.4654592621819,5.72742209646294,339.018614070817));
#14132=CARTESIAN_POINT('Ctrl Pts',(91.187221227908,6.47877504132782,332.358391231638));
#14133=CARTESIAN_POINT('Ctrl Pts',(90.9089831936341,1.28465175732854,328.122333769104));
#14134=CARTESIAN_POINT('Ctrl Pts',(90.6532601192325,-4.57267337374315,330.029862090751));
#14135=CARTESIAN_POINT('Ctrl Pts',(90.4902830562557,-5.90248644698631,333.513572395831));
#14136=CARTESIAN_POINT('Ctrl Pts',(90.4200520047035,-5.91614342231082,335.00545103649));
#14137=CARTESIAN_POINT('',(88.6700510690619,-5.92177106793959,334.998328828675));
#14138=CARTESIAN_POINT('Ctrl Pts',(90.420051987023,-5.91674748815069,335.005451968678));
#14139=CARTESIAN_POINT('Ctrl Pts',(90.4104409465018,-5.91655934632297,335.209632834768));
#14140=CARTESIAN_POINT('Ctrl Pts',(90.4008299059805,-5.90579871717187,335.413343160755));
#14141=CARTESIAN_POINT('Ctrl Pts',(90.3912188654592,-5.88463187011856,335.615660877176));
#14142=CARTESIAN_POINT('Ctrl Pts',(90.3813759739492,-5.86295440671688,335.822859185085));
#14143=CARTESIAN_POINT('Ctrl Pts',(90.3715330824393,-5.83036257602901,336.028597195015));
#14144=CARTESIAN_POINT('Ctrl Pts',(90.3616901909294,-5.78708280121524,336.231910392187));
#14145=CARTESIAN_POINT('Ctrl Pts',(90.3586291689817,-5.7736233070752,336.295138373333));
#14146=CARTESIAN_POINT('Ctrl Pts',(90.3555681470339,-5.75913048755993,336.35813200794));
#14147=CARTESIAN_POINT('Ctrl Pts',(90.3525071250861,-5.74361208103852,336.420862704503));
#14148=CARTESIAN_POINT('Ctrl Pts',(90.3450831476481,-5.70597487952363,336.573005120961));
#14149=CARTESIAN_POINT('Ctrl Pts',(90.3376591702101,-5.66223157998761,336.723880562478));
#14150=CARTESIAN_POINT('Ctrl Pts',(90.3302351927721,-5.61248137558281,336.872961123792));
#14151=CARTESIAN_POINT('Ctrl Pts',(90.3228199767445,-5.56278988390454,337.021865747613));
#14152=CARTESIAN_POINT('Ctrl Pts',(90.3154047607168,-5.50710571521944,337.168979357021));
#14153=CARTESIAN_POINT('Ctrl Pts',(90.3079895446892,-5.44557886855915,337.313785069708));
#14154=CARTESIAN_POINT('Ctrl Pts',(90.3005814635451,-5.38411122272096,337.458451451066));
#14155=CARTESIAN_POINT('Ctrl Pts',(90.293173382401,-5.31681223582546,337.600814015401));
#14156=CARTESIAN_POINT('Ctrl Pts',(90.2857653012568,-5.24388138932037,337.740371970598));
#14157=CARTESIAN_POINT('Ctrl Pts',(90.2783627340828,-5.17100482657627,337.87982605026));
#14158=CARTESIAN_POINT('Ctrl Pts',(90.2709601669088,-5.0925049230122,338.016479347992));
#14159=CARTESIAN_POINT('Ctrl Pts',(90.2635575997348,-5.00862880601297,338.149852067332));
#14160=CARTESIAN_POINT('Ctrl Pts',(90.2561589299801,-4.92479684942301,338.283154566518));
#14161=CARTESIAN_POINT('Ctrl Pts',(90.2487602602254,-4.83559451479498,338.413179612019));
#14162=CARTESIAN_POINT('Ctrl Pts',(90.2413615904706,-4.74131424553725,338.539473094624));
#14163=CARTESIAN_POINT('Ctrl Pts',(90.2339641412667,-4.64704952959606,338.665745742726));
#14164=CARTESIAN_POINT('Ctrl Pts',(90.2265666920627,-4.54770876463457,338.788287750904));
#14165=CARTESIAN_POINT('Ctrl Pts',(90.2191692428587,-4.4436270590002,338.906674944633));
#14166=CARTESIAN_POINT('Ctrl Pts',(90.2117721143952,-4.33954986616713,339.025057005299));
#14167=CARTESIAN_POINT('Ctrl Pts',(90.2043749859318,-4.23073238780169,339.139284329412));
#14168=CARTESIAN_POINT('Ctrl Pts',(90.1969778574683,-4.11754908880057,339.248966940777));
#14169=CARTESIAN_POINT('Ctrl Pts',(90.1895795900317,-4.00434836239684,339.358666440527));
#14170=CARTESIAN_POINT('Ctrl Pts',(90.1821813225951,-3.88678074489291,339.463819574451));
#14171=CARTESIAN_POINT('Ctrl Pts',(90.1747830551585,-3.76525639929152,339.564074365092));
#14172=CARTESIAN_POINT('Ctrl Pts',(90.1673821886327,-3.6436893609092,339.664364376297));
#14173=CARTESIAN_POINT('Ctrl Pts',(90.1599813221069,-3.51816311456883,339.759752380678));
#14174=CARTESIAN_POINT('Ctrl Pts',(90.1525804555812,-3.3891194882614,339.849927799131));
#14175=CARTESIAN_POINT('Ctrl Pts',(90.1451714621964,-3.25993415971541,339.940202238815));
#14176=CARTESIAN_POINT('Ctrl Pts',(90.1377624688116,-3.12722404384612,340.025252447698));
#14177=CARTESIAN_POINT('Ctrl Pts',(90.1303534754269,-2.99145904998252,340.104811780544));
#14178=CARTESIAN_POINT('Ctrl Pts',(90.1229399178466,-2.85561042019957,340.184420124683));
#14179=CARTESIAN_POINT('Ctrl Pts',(90.1155263602664,-2.71670349097573,340.258530677302));
#14180=CARTESIAN_POINT('Ctrl Pts',(90.1081128026861,-2.57523068084449,340.326923831156));
#14181=CARTESIAN_POINT('Ctrl Pts',(90.1006886905494,-2.43355645826807,340.395414355186));
#14182=CARTESIAN_POINT('Ctrl Pts',(90.0932645784127,-2.28930940031275,340.458171075227));
#14183=CARTESIAN_POINT('Ctrl Pts',(90.085840466276,-2.14300046696549,340.515023078926));
#14184=CARTESIAN_POINT('Ctrl Pts',(90.0819833411215,-2.06698708559968,340.544559983746));
#14185=CARTESIAN_POINT('Ctrl Pts',(90.0781262159669,-1.9904173953332,340.572503901069));
#14186=CARTESIAN_POINT('Ctrl Pts',(90.0742690908124,-1.91336430444853,340.598836272027));
#14187=CARTESIAN_POINT('Ctrl Pts',(90.0668451133744,-1.7650568512715,340.649519337794));
#14188=CARTESIAN_POINT('Ctrl Pts',(90.0594211359363,-1.61451046434392,340.694382022628));
#14189=CARTESIAN_POINT('Ctrl Pts',(90.0519971584983,-1.46222274957149,340.733222060337));
#14190=CARTESIAN_POINT('Ctrl Pts',(90.0445819424707,-1.3101147572153,340.772016260958));
#14191=CARTESIAN_POINT('Ctrl Pts',(90.037166726443,-1.1562698857,340.804801870969));
#14192=CARTESIAN_POINT('Ctrl Pts',(90.0297515104154,-1.00120396546976,340.83142531308));
#14193=CARTESIAN_POINT('Ctrl Pts',(90.0223434292713,-0.846287248887313,
340.858023138248));
#14194=CARTESIAN_POINT('Ctrl Pts',(90.0149353481272,-0.690152187941684,
340.878470536731));
#14195=CARTESIAN_POINT('Ctrl Pts',(90.007527266983,-0.533327860263088,340.892664249384));
#14196=CARTESIAN_POINT('Ctrl Pts',(90.000124699809,-0.376620259795989,340.906847397398));
#14197=CARTESIAN_POINT('Ctrl Pts',(89.992722132635,-0.219224784220909,340.914786094336));
#14198=CARTESIAN_POINT('Ctrl Pts',(89.985319565461,-0.0616786394269871,
340.916428509493));
#14199=CARTESIAN_POINT('Ctrl Pts',(89.9779208957063,0.0957845580107002,
340.918070059925));
#14200=CARTESIAN_POINT('Ctrl Pts',(89.9705222259515,0.253397894432321,340.913421926644));
#14201=CARTESIAN_POINT('Ctrl Pts',(89.9631235561967,0.410621241804524,340.902484287));
#14202=CARTESIAN_POINT('Ctrl Pts',(89.9557261069927,0.567818652206232,340.891548451726));
#14203=CARTESIAN_POINT('Ctrl Pts',(89.9483286577887,0.724625829295427,340.874325195212));
#14204=CARTESIAN_POINT('Ctrl Pts',(89.9409312085847,0.880504729307353,340.85086677204));
#14205=CARTESIAN_POINT('Ctrl Pts',(89.9335340801212,1.03637687068193,340.827409365985));
#14206=CARTESIAN_POINT('Ctrl Pts',(89.9261369516578,1.1913204459509,340.797717386349));
#14207=CARTESIAN_POINT('Ctrl Pts',(89.9187398231943,1.34480487136977,340.761894690155));
#14208=CARTESIAN_POINT('Ctrl Pts',(89.9113415557576,1.49831292955868,340.726066478161));
#14209=CARTESIAN_POINT('Ctrl Pts',(89.903943288321,1.65036102707908,340.684105754859));
#14210=CARTESIAN_POINT('Ctrl Pts',(89.8965450208844,1.80043121584224,340.636166959869));
#14211=CARTESIAN_POINT('Ctrl Pts',(89.8891441543587,1.95055412584089,340.588211323477));
#14212=CARTESIAN_POINT('Ctrl Pts',(89.8817432878329,2.09869738832798,340.534273547477));
#14213=CARTESIAN_POINT('Ctrl Pts',(89.8743424213071,2.24436073222976,340.47455710228));
#14214=CARTESIAN_POINT('Ctrl Pts',(89.8669334279223,2.39018402840932,340.414775082717));
#14215=CARTESIAN_POINT('Ctrl Pts',(89.8595244345375,2.53352162212728,340.349201863242));
#14216=CARTESIAN_POINT('Ctrl Pts',(89.8521154411528,2.67389499081471,340.2780883036));
#14217=CARTESIAN_POINT('Ctrl Pts',(89.8447018835725,2.81435483433905,340.206930935551));
#14218=CARTESIAN_POINT('Ctrl Pts',(89.8372883259923,2.95184648899596,340.130226607802));
#14219=CARTESIAN_POINT('Ctrl Pts',(89.8298747684121,3.08591880644607,340.048270563522));
#14220=CARTESIAN_POINT('Ctrl Pts',(89.8224506562754,3.22018200038529,339.966197839809));
#14221=CARTESIAN_POINT('Ctrl Pts',(89.8150265441386,3.35101582507747,339.878858673592));
#14222=CARTESIAN_POINT('Ctrl Pts',(89.8076024320019,3.4780000469114,339.786590251545));
#14223=CARTESIAN_POINT('Ctrl Pts',(89.8037453068474,3.54397346262093,339.738653091505));
#14224=CARTESIAN_POINT('Ctrl Pts',(89.7998881816928,3.60890835182653,339.689386062502));
#14225=CARTESIAN_POINT('Ctrl Pts',(89.7960310565382,3.67274965312461,339.638840431398));
#14226=CARTESIAN_POINT('Ctrl Pts',(89.7886070791002,3.79562779719748,339.541553045101));
#14227=CARTESIAN_POINT('Ctrl Pts',(89.7811831016622,3.91482307429404,339.439233149551));
#14228=CARTESIAN_POINT('Ctrl Pts',(89.7737591242242,4.02989611135027,339.332189734329));
#14229=CARTESIAN_POINT('Ctrl Pts',(89.7663439081966,4.14483334490911,339.225272646442));
#14230=CARTESIAN_POINT('Ctrl Pts',(89.7589286921689,4.25565775141133,339.113643386663));
#14231=CARTESIAN_POINT('Ctrl Pts',(89.7515134761413,4.36196103898518,338.997652618334));
#14232=CARTESIAN_POINT('Ctrl Pts',(89.7441053949972,4.46816204207088,338.881773455739));
#14233=CARTESIAN_POINT('Ctrl Pts',(89.7366973138531,4.56985033618628,338.761541412585));
#14234=CARTESIAN_POINT('Ctrl Pts',(89.729289232709,4.66665277425075,338.637345522091));
#14235=CARTESIAN_POINT('Ctrl Pts',(89.721886665535,4.76338316049274,338.513242072867));
#14236=CARTESIAN_POINT('Ctrl Pts',(89.714484098361,4.85523470329714,338.385180944007));
#14237=CARTESIAN_POINT('Ctrl Pts',(89.707081531187,4.94187310418581,338.253585834833));
#14238=CARTESIAN_POINT('Ctrl Pts',(89.6996828614322,5.02846589033494,338.122060009909));
#14239=CARTESIAN_POINT('Ctrl Pts',(89.6922841916775,5.10985079608434,337.987004221151));
#14240=CARTESIAN_POINT('Ctrl Pts',(89.6848855219227,5.18573567629961,337.84887276972));
#14241=CARTESIAN_POINT('Ctrl Pts',(89.6774880727187,5.26160803786605,337.710764105689));
#14242=CARTESIAN_POINT('Ctrl Pts',(89.6700906235148,5.33198199513823,337.569581112771));
#14243=CARTESIAN_POINT('Ctrl Pts',(89.6626931743108,5.39661032375546,337.425804521398));
#14244=CARTESIAN_POINT('Ctrl Pts',(89.6552960458473,5.46123585020104,337.282034163928));
#14245=CARTESIAN_POINT('Ctrl Pts',(89.6478989173839,5.52011609031253,337.135670772002));
#14246=CARTESIAN_POINT('Ctrl Pts',(89.6405017889204,5.57305125036858,336.987216727804));
#14247=CARTESIAN_POINT('Ctrl Pts',(89.6331035214838,5.62599456111788,336.83873982539));
#14248=CARTESIAN_POINT('Ctrl Pts',(89.6257052540472,5.67299084378648,336.688171981297));
#14249=CARTESIAN_POINT('Ctrl Pts',(89.6183069866105,5.71388967851577,336.536032325262));
#14250=CARTESIAN_POINT('Ctrl Pts',(89.6109061200848,5.7548028814358,336.383839220967));
#14251=CARTESIAN_POINT('Ctrl Pts',(89.603505253559,5.78961427467648,336.230073565502));
#14252=CARTESIAN_POINT('Ctrl Pts',(89.5961043870333,5.81822423546171,336.075266156998));
#14253=CARTESIAN_POINT('Ctrl Pts',(89.5886953936485,5.84686561271912,335.92028875516));
#14254=CARTESIAN_POINT('Ctrl Pts',(89.5812864002637,5.86929189019015,335.764267682981));
#14255=CARTESIAN_POINT('Ctrl Pts',(89.573877406879,5.88545506516443,335.6077410949));
#14256=CARTESIAN_POINT('Ctrl Pts',(89.5664638492987,5.90162819721203,335.451118081041));
#14257=CARTESIAN_POINT('Ctrl Pts',(89.5590502917185,5.91153051519712,335.293989302346));
#14258=CARTESIAN_POINT('Ctrl Pts',(89.5516367341382,5.91516615314655,335.136893912098));
#14259=CARTESIAN_POINT('Ctrl Pts',(89.5442126220015,5.9188069670922,334.979574867801));
#14260=CARTESIAN_POINT('Ctrl Pts',(89.5367885098648,5.91616328870546,334.822289679041));
#14261=CARTESIAN_POINT('Ctrl Pts',(89.5293643977281,5.90729125293326,334.66557420028));
#14262=CARTESIAN_POINT('Ctrl Pts',(89.5255072725736,5.90268187315569,334.584154199597));
#14263=CARTESIAN_POINT('Ctrl Pts',(89.521650147419,5.89639217191359,334.502887849604));
#14264=CARTESIAN_POINT('Ctrl Pts',(89.5177930222644,5.88843546371964,334.421849196049));
#14265=CARTESIAN_POINT('Ctrl Pts',(89.5103690448264,5.87312083955135,334.265870556134));
#14266=CARTESIAN_POINT('Ctrl Pts',(89.5029450673884,5.85158126034507,334.110265538108));
#14267=CARTESIAN_POINT('Ctrl Pts',(89.4955210899504,5.82383879205416,333.955570832146));
#14268=CARTESIAN_POINT('Ctrl Pts',(89.4881058739228,5.79612906404991,333.801058689211));
#14269=CARTESIAN_POINT('Ctrl Pts',(89.4806906578952,5.76223108345799,333.647455083697));
#14270=CARTESIAN_POINT('Ctrl Pts',(89.4732754418676,5.72221878040337,333.495293121004));
#14271=CARTESIAN_POINT('Ctrl Pts',(89.4658673607235,5.68224497698528,333.343277567785));
#14272=CARTESIAN_POINT('Ctrl Pts',(89.4584592795794,5.636168657678,333.192701254375));
#14273=CARTESIAN_POINT('Ctrl Pts',(89.4510511984353,5.58411503751873,333.044088496312));
#14274=CARTESIAN_POINT('Ctrl Pts',(89.4436486312613,5.53210016181966,332.89558635344));
#14275=CARTESIAN_POINT('Ctrl Pts',(89.4362460640873,5.47411696674855,332.749045206557));
#14276=CARTESIAN_POINT('Ctrl Pts',(89.4288434969133,5.41034084201738,332.604975462402));
#14277=CARTESIAN_POINT('Ctrl Pts',(89.4214448271586,5.34659829513706,332.460981570336));
#14278=CARTESIAN_POINT('Ctrl Pts',(89.4140461574039,5.277069043448,332.319456830024));
#14279=CARTESIAN_POINT('Ctrl Pts',(89.4066474876491,5.20197702199252,332.180892760968));
#14280=CARTESIAN_POINT('Ctrl Pts',(89.3992500384452,5.12689738838885,332.042351550681));
#14281=CARTESIAN_POINT('Ctrl Pts',(89.3918525892412,5.04625698397372,331.906770370101));
#14282=CARTESIAN_POINT('Ctrl Pts',(89.3844551400372,4.96032627793727,331.774617266292));
#14283=CARTESIAN_POINT('Ctrl Pts',(89.3770580115738,4.87439929770649,331.64246989241));
#14284=CARTESIAN_POINT('Ctrl Pts',(89.3696608831103,4.78318267538167,331.513750612644));
#14285=CARTESIAN_POINT('Ctrl Pts',(89.3622637546468,4.6869907550137,331.388899305625));
#14286=CARTESIAN_POINT('Ctrl Pts',(89.3548654872102,4.59078402349128,331.264028774621));
#14287=CARTESIAN_POINT('Ctrl Pts',(89.3474672197737,4.48960069636764,331.143027697883));
#14288=CARTESIAN_POINT('Ctrl Pts',(89.3400689523371,4.38379592009836,331.026303497569));
#14289=CARTESIAN_POINT('Ctrl Pts',(89.3326680858113,4.27795397349836,330.909538290816));
#14290=CARTESIAN_POINT('Ctrl Pts',(89.3252672192856,4.16748759573141,330.797053228328));
#14291=CARTESIAN_POINT('Ctrl Pts',(89.3178663527598,4.05278923467022,330.689219330348));
#14292=CARTESIAN_POINT('Ctrl Pts',(89.3104573593751,3.937964923843,330.58126702044));
#14293=CARTESIAN_POINT('Ctrl Pts',(89.3030483659903,3.81889962124384,330.477976330628));
#14294=CARTESIAN_POINT('Ctrl Pts',(89.2956393726056,3.69601989539976,330.379678853661));
#14295=CARTESIAN_POINT('Ctrl Pts',(89.2882258150254,3.57306447140599,330.281320822058));
#14296=CARTESIAN_POINT('Ctrl Pts',(89.2808122574451,3.44629024166273,330.187962353408));
#14297=CARTESIAN_POINT('Ctrl Pts',(89.2733986998649,3.31615282882766,330.099891738098));
#14298=CARTESIAN_POINT('Ctrl Pts',(89.2659745877282,3.18583014156066,330.011695738144));
#14299=CARTESIAN_POINT('Ctrl Pts',(89.2585504755915,3.05213502473042,329.928802823039));
#14300=CARTESIAN_POINT('Ctrl Pts',(89.2511263634548,2.91554846762974,329.851455769307));
#14301=CARTESIAN_POINT('Ctrl Pts',(89.2472692383,2.8445862521478,329.811270860848));
#14302=CARTESIAN_POINT('Ctrl Pts',(89.2434121131452,2.77284392644715,329.772582119761));
#14303=CARTESIAN_POINT('Ctrl Pts',(89.2395549879904,2.70039096242497,329.735418419993));
#14304=CARTESIAN_POINT('Ctrl Pts',(89.2321310105524,2.56093757457113,329.663887822068));
#14305=CARTESIAN_POINT('Ctrl Pts',(89.2247070331144,2.41842969297576,329.597794109881));
#14306=CARTESIAN_POINT('Ctrl Pts',(89.2172830556764,2.27333057300988,329.53740916155));
#14307=CARTESIAN_POINT('Ctrl Pts',(89.2098678396487,2.12840269183701,329.477095476543));
#14308=CARTESIAN_POINT('Ctrl Pts',(89.2024526236211,1.98089000060662,329.422477286888));
#14309=CARTESIAN_POINT('Ctrl Pts',(89.1950374075934,1.83128080685596,329.373780917086));
#14310=CARTESIAN_POINT('Ctrl Pts',(89.1876293264493,1.68181556631823,329.325131402687));
#14311=CARTESIAN_POINT('Ctrl Pts',(89.1802212453053,1.53025819173092,329.282392479334));
#14312=CARTESIAN_POINT('Ctrl Pts',(89.1728131641612,1.3771173522576,329.245742588256));
#14313=CARTESIAN_POINT('Ctrl Pts',(89.1654105969871,1.22409049830801,329.209119976361));
#14314=CARTESIAN_POINT('Ctrl Pts',(89.1580080298131,1.06948288764735,329.178577459006));
#14315=CARTESIAN_POINT('Ctrl Pts',(89.1506054626391,0.913818645627798,329.154243757613));
#14316=CARTESIAN_POINT('Ctrl Pts',(89.1432067928844,0.758236360151347,329.129922867808));
#14317=CARTESIAN_POINT('Ctrl Pts',(89.1358081231296,0.60159891904849,329.111804341225));
#14318=CARTESIAN_POINT('Ctrl Pts',(89.1284094533749,0.444440835655226,329.099965855514));
#14319=CARTESIAN_POINT('Ctrl Pts',(89.1210120041709,0.287308678465478,329.088129322786));
#14320=CARTESIAN_POINT('Ctrl Pts',(89.1136145549669,0.129656421243884,329.082570802788));
#14321=CARTESIAN_POINT('Ctrl Pts',(89.106217105763,-0.0279759788522484,
329.08331613933));
#14322=CARTESIAN_POINT('Ctrl Pts',(89.0988199772995,-0.185601544282214,
329.084061443556));
#14323=CARTESIAN_POINT('Ctrl Pts',(89.091422848836,-0.343206881091485,329.091110059099));
#14324=CARTESIAN_POINT('Ctrl Pts',(89.0840257203725,-0.500251976352694,
329.104435690907));
#14325=CARTESIAN_POINT('Ctrl Pts',(89.0766274529359,-0.657321252638202,
329.117763374529));
#14326=CARTESIAN_POINT('Ctrl Pts',(89.0692291854993,-0.813829743716658,
329.137369967296));
#14327=CARTESIAN_POINT('Ctrl Pts',(89.0618309180627,-0.969242649478629,
329.163177298484));
#14328=CARTESIAN_POINT('Ctrl Pts',(89.0544300515369,-1.12471015342897,329.188993696059));
#14329=CARTESIAN_POINT('Ctrl Pts',(89.0470291850112,-1.27908093780846,329.221015108116));
#14330=CARTESIAN_POINT('Ctrl Pts',(89.0396283184854,-1.43183062771581,329.259112297211));
#14331=CARTESIAN_POINT('Ctrl Pts',(89.0322193251006,-1.58474805138602,329.297251320661));
#14332=CARTESIAN_POINT('Ctrl Pts',(89.0248103317159,-1.73604046326154,329.341479354688));
#14333=CARTESIAN_POINT('Ctrl Pts',(89.0174013383311,-1.88519817921912,329.39161713258));
#14334=CARTESIAN_POINT('Ctrl Pts',(89.0099877807509,-2.03444778147482,329.441785797073));
#14335=CARTESIAN_POINT('Ctrl Pts',(89.0025742231706,-2.18155971949618,329.49787132718));
#14336=CARTESIAN_POINT('Ctrl Pts',(88.9951606655904,-2.32604500018266,329.559646590558));
#14337=CARTESIAN_POINT('Ctrl Pts',(88.9877365534537,-2.47073598211767,329.621509802334));
#14338=CARTESIAN_POINT('Ctrl Pts',(88.980312441317,-2.61279250201358,329.689078765579));
#14339=CARTESIAN_POINT('Ctrl Pts',(88.9728883291803,-2.75175011300632,329.762080386444));
#14340=CARTESIAN_POINT('Ctrl Pts',(88.9690312040257,-2.82394418644098,329.800007667577));
#14341=CARTESIAN_POINT('Ctrl Pts',(88.9651740788711,-2.89530226321513,329.83940062205));
#14342=CARTESIAN_POINT('Ctrl Pts',(88.9613169537165,-2.96576246738171,329.880216454813));
#14343=CARTESIAN_POINT('Ctrl Pts',(88.9538929762785,-3.10138030321598,329.958776472805));
#14344=CARTESIAN_POINT('Ctrl Pts',(88.9464689988405,-3.23407910767295,330.04284729059));
#14345=CARTESIAN_POINT('Ctrl Pts',(88.9390450214025,-3.36337955858028,330.132186475693));
#14346=CARTESIAN_POINT('Ctrl Pts',(88.9316298053749,-3.49252741550123,330.221420227116));
#14347=CARTESIAN_POINT('Ctrl Pts',(88.9242145893472,-3.61828459791148,330.315909759804));
#14348=CARTESIAN_POINT('Ctrl Pts',(88.9167993733196,-3.74019653348104,330.415366922704));
#14349=CARTESIAN_POINT('Ctrl Pts',(88.9093912921755,-3.86199116600011,330.514728388423));
#14350=CARTESIAN_POINT('Ctrl Pts',(88.9019832110314,-3.97994763019167,330.619047734263));
#14351=CARTESIAN_POINT('Ctrl Pts',(88.8945751298873,-4.09364060094926,330.72799377426));
#14352=CARTESIAN_POINT('Ctrl Pts',(88.8871725627133,-4.20724894795202,330.836858723729));
#14353=CARTESIAN_POINT('Ctrl Pts',(88.8797699955393,-4.31659985190306,330.950343253272));
#14354=CARTESIAN_POINT('Ctrl Pts',(88.8723674283653,-4.4213014339096,331.068076273246));
#14355=CARTESIAN_POINT('Ctrl Pts',(88.8649687586106,-4.52594789099111,331.1857473073));
#14356=CARTESIAN_POINT('Ctrl Pts',(88.8575700888559,-4.6259496537724,331.307662098862));
#14357=CARTESIAN_POINT('Ctrl Pts',(88.8501714191011,-4.72095214562284,331.433413200097));
#14358=CARTESIAN_POINT('Ctrl Pts',(88.8427739698971,-4.81593896501203,331.559143556306));
#14359=CARTESIAN_POINT('Ctrl Pts',(88.8353765206932,-4.90592792553089,331.688708668649));
#14360=CARTESIAN_POINT('Ctrl Pts',(88.8279790714892,-4.99060509276845,331.8216684612));
#14361=CARTESIAN_POINT('Ctrl Pts',(88.8205819430257,-5.07527858855166,331.954622488846));
#14362=CARTESIAN_POINT('Ctrl Pts',(88.8131848145622,-5.15464054850606,332.09097058925));
#14363=CARTESIAN_POINT('Ctrl Pts',(88.8057876860988,-5.2284208527207,332.230244424261));
#14364=CARTESIAN_POINT('Ctrl Pts',(88.7983894186622,-5.30221251726033,332.369539703966));
#14365=CARTESIAN_POINT('Ctrl Pts',(88.7909911512256,-5.37042064009199,332.511761285448));
#14366=CARTESIAN_POINT('Ctrl Pts',(88.783592883789,-5.43282154561915,332.656417141222));
#14367=CARTESIAN_POINT('Ctrl Pts',(88.7761920172632,-5.49524437324065,332.80112381612));
#14368=CARTESIAN_POINT('Ctrl Pts',(88.7687911507375,-5.55185577391612,332.948266125513));
#14369=CARTESIAN_POINT('Ctrl Pts',(88.7613902842117,-5.60248065682288,333.097333173563));
#14370=CARTESIAN_POINT('Ctrl Pts',(88.753981290827,-5.65316113069103,333.246563911482));
#14371=CARTESIAN_POINT('Ctrl Pts',(88.7465722974422,-5.69784183853674,333.397723255326));
#14372=CARTESIAN_POINT('Ctrl Pts',(88.7391633040575,-5.73639771023748,333.550285589338));
#14373=CARTESIAN_POINT('Ctrl Pts',(88.7317497464772,-5.7749773336851,333.702941907009));
#14374=CARTESIAN_POINT('Ctrl Pts',(88.724336188897,-5.80742452583055,333.857002572714));
#14375=CARTESIAN_POINT('Ctrl Pts',(88.7169226313168,-5.83366566488127,334.011933467379));
#14376=CARTESIAN_POINT('Ctrl Pts',(88.7094985191801,-5.85994416299754,334.167084934537));
#14377=CARTESIAN_POINT('Ctrl Pts',(88.7020744070434,-5.87999891440106,334.323108735878));
#14378=CARTESIAN_POINT('Ctrl Pts',(88.6946502949067,-5.89380823068842,334.479466521375));
#14379=CARTESIAN_POINT('Ctrl Pts',(88.690793169752,-5.900982726472,334.560700686009));
#14380=CARTESIAN_POINT('Ctrl Pts',(88.6869360445973,-5.9064723005119,334.642025003162));
#14381=CARTESIAN_POINT('Ctrl Pts',(88.6830789194426,-5.9102794554545,334.72336428117));
#14382=CARTESIAN_POINT('Ctrl Pts',(88.6787366145296,-5.91456550450621,334.81493505794));
#14383=CARTESIAN_POINT('Ctrl Pts',(88.6743943096166,-5.91672357262935,334.906606214109));
#14384=CARTESIAN_POINT('Ctrl Pts',(88.6700520047036,-5.91674975877771,334.998310472272));
#14385=CARTESIAN_POINT('',(86.9200532024049,-5.91345947321307,334.995429316743));
#14386=CARTESIAN_POINT('Ctrl Pts',(88.6700502969966,-5.92591451127428,334.998343975863));
#14387=CARTESIAN_POINT('Ctrl Pts',(88.5816471597205,-5.91883322604964,336.868206066303));
#14388=CARTESIAN_POINT('Ctrl Pts',(88.4004980110199,-3.95334079215119,340.712572307138));
#14389=CARTESIAN_POINT('Ctrl Pts',(88.1266028508947,2.5977797484408,341.496473143162));
#14390=CARTESIAN_POINT('Ctrl Pts',(87.8483648166207,6.86883054471249,336.331085973649));
#14391=CARTESIAN_POINT('Ctrl Pts',(87.5701267823467,4.83645693387304,329.944180852918));
#14392=CARTESIAN_POINT('Ctrl Pts',(87.2918887480729,-1.63426181919367,328.196926339695));
#14393=CARTESIAN_POINT('Ctrl Pts',(87.075197847428,-5.50564593875477,331.698261224195));
#14394=CARTESIAN_POINT('Ctrl Pts',(86.9512529582079,-5.91578097000932,334.331223968412));
#14395=CARTESIAN_POINT('Ctrl Pts',(86.9200540804124,-5.91104854439068,334.995412478147));
#14396=CARTESIAN_POINT('',(85.1700508174281,-5.91265977156438,335.003771382507));
#14397=CARTESIAN_POINT('Ctrl Pts',(86.9200520047035,-5.91674825227522,334.995452286488));
#14398=CARTESIAN_POINT('Ctrl Pts',(86.9123586994878,-5.9168742583105,335.15939093106));
#14399=CARTESIAN_POINT('Ctrl Pts',(86.904665394272,-5.91018172402343,335.323406540034));
#14400=CARTESIAN_POINT('Ctrl Pts',(86.8969720890562,-5.89668281031374,335.486890539085));
#14401=CARTESIAN_POINT('Ctrl Pts',(86.8895765307271,-5.88370633259449,335.644047367906));
#14402=CARTESIAN_POINT('Ctrl Pts',(86.882180972398,-5.8644404998989,335.800712565962));
#14403=CARTESIAN_POINT('Ctrl Pts',(86.8747854140689,-5.83894918947698,335.956348746643));
#14404=CARTESIAN_POINT('Ctrl Pts',(86.8673893946862,-5.81345628987677,336.111994629989));
#14405=CARTESIAN_POINT('Ctrl Pts',(86.8599933753034,-5.78173719942712,336.266611000192));
#14406=CARTESIAN_POINT('Ctrl Pts',(86.8525973559207,-5.74390721152469,336.419669154379));
#14407=CARTESIAN_POINT('Ctrl Pts',(86.8451994203594,-5.70606742253748,336.572766963242));
#14408=CARTESIAN_POINT('Ctrl Pts',(86.837801484798,-5.66211367295776,336.724305390377));
#14409=CARTESIAN_POINT('Ctrl Pts',(86.8304035492367,-5.61221152486639,336.873769559646));
#14410=CARTESIAN_POINT('Ctrl Pts',(86.8230022415009,-5.56228663005751,337.023301858632));
#14411=CARTESIAN_POINT('Ctrl Pts',(86.8156009337651,-5.50640805566121,337.170757663903));
#14412=CARTESIAN_POINT('Ctrl Pts',(86.8081996260293,-5.44478995781093,337.315640921607));
#14413=CARTESIAN_POINT('Ctrl Pts',(86.8007894619212,-5.38309812801616,337.460697545979));
#14414=CARTESIAN_POINT('Ctrl Pts',(86.7933792978132,-5.31565320750368,337.603175133357));
#14415=CARTESIAN_POINT('Ctrl Pts',(86.7859691337051,-5.24271620041503,337.742600482098));
#14416=CARTESIAN_POINT('Ctrl Pts',(86.7785537337463,-5.16972765772175,337.88212434557));
#14417=CARTESIAN_POINT('Ctrl Pts',(86.7711383337874,-5.0912394818629,338.018591351566));
#14418=CARTESIAN_POINT('Ctrl Pts',(86.7637229338285,-5.00755637960994,338.151556705428));
#14419=CARTESIAN_POINT('Ctrl Pts',(86.7562969808181,-4.92375418572361,338.284711285797));
#14420=CARTESIAN_POINT('Ctrl Pts',(86.7488710278077,-4.83474251551918,338.414353959321));
#14421=CARTESIAN_POINT('Ctrl Pts',(86.7414450747972,-4.74086715485042,338.54007191771));
#14422=CARTESIAN_POINT('Ctrl Pts',(86.7394342763732,-4.71544759899988,338.574113807317));
#14423=CARTESIAN_POINT('Ctrl Pts',(86.7374234779491,-4.68967164190016,338.60786813478));
#14424=CARTESIAN_POINT('Ctrl Pts',(86.7354126795251,-4.663546611525,338.641327170776));
#14425=CARTESIAN_POINT('Ctrl Pts',(86.727988702087,-4.5670915746845,338.764859756322));
#14426=CARTESIAN_POINT('Ctrl Pts',(86.720564724649,-4.4655792630452,338.884743557117));
#14427=CARTESIAN_POINT('Ctrl Pts',(86.713140747211,-4.35931569085774,339.00053712268));
#14428=CARTESIAN_POINT('Ctrl Pts',(86.7057255311833,-4.25317752567361,339.116194034414));
#14429=CARTESIAN_POINT('Ctrl Pts',(86.6983103151557,-4.14229951105499,339.227770047022));
#14430=CARTESIAN_POINT('Ctrl Pts',(86.6908950991281,-4.02702954403851,339.33485450897));
#14431=CARTESIAN_POINT('Ctrl Pts',(86.6834870179839,-3.91187048920382,339.441835934788));
#14432=CARTESIAN_POINT('Ctrl Pts',(86.6760789368398,-3.79232816658171,339.544334161424));
#14433=CARTESIAN_POINT('Ctrl Pts',(86.6686708556957,-3.66878907963946,339.641973422115));
#14434=CARTESIAN_POINT('Ctrl Pts',(86.6612682885216,-3.54534194509598,339.739540008121));
#14435=CARTESIAN_POINT('Ctrl Pts',(86.6538657213476,-3.41790426116913,339.832254598968));
#14436=CARTESIAN_POINT('Ctrl Pts',(86.6464631541736,-3.28689745908954,339.919780041418));
#14437=CARTESIAN_POINT('Ctrl Pts',(86.6390644844188,-3.15595963151851,340.007259402104));
#14438=CARTESIAN_POINT('Ctrl Pts',(86.6316658146641,-3.02145673772766,340.089554848654));
#14439=CARTESIAN_POINT('Ctrl Pts',(86.6242671449093,-2.88384109486179,340.166371173472));
#14440=CARTESIAN_POINT('Ctrl Pts',(86.6168696957053,-2.74624815430399,340.243174825982));
#14441=CARTESIAN_POINT('Ctrl Pts',(86.6094722465013,-2.60554380937926,340.314500968952));
#14442=CARTESIAN_POINT('Ctrl Pts',(86.6020747972973,-2.46220710937423,340.380099135987));
#14443=CARTESIAN_POINT('Ctrl Pts',(86.5946776688338,-2.31887662419832,340.4456944588));
#14444=CARTESIAN_POINT('Ctrl Pts',(86.5872805403703,-2.17291435023966,340.50556214418));
#14445=CARTESIAN_POINT('Ctrl Pts',(86.5798834119068,-2.02482130847057,340.559499009017));
#14446=CARTESIAN_POINT('Ctrl Pts',(86.5724851444701,-1.87670546406953,340.613444178785));
#14447=CARTESIAN_POINT('Ctrl Pts',(86.5650868770335,-1.72645854929582,340.661456581983));
#14448=CARTESIAN_POINT('Ctrl Pts',(86.5576886095969,-1.57459866584797,340.703382295096));
#14449=CARTESIAN_POINT('Ctrl Pts',(86.5502877430711,-1.42268543242737,340.745322737151));
#14450=CARTESIAN_POINT('Ctrl Pts',(86.5428868765454,-1.26915846165383,340.781172132474));
#14451=CARTESIAN_POINT('Ctrl Pts',(86.5354860100196,-1.11454786652365,340.810827274642));
#14452=CARTESIAN_POINT('Ctrl Pts',(86.5280770166348,-0.959767494177773,
340.840514980992));
#14453=CARTESIAN_POINT('Ctrl Pts',(86.5206680232501,-0.803901487883792,
340.86399478012));
#14454=CARTESIAN_POINT('Ctrl Pts',(86.5132590298653,-0.647487665506531,
340.881215034797));
#14455=CARTESIAN_POINT('Ctrl Pts',(86.505845472285,-0.490977486819397,340.898445897743));
#14456=CARTESIAN_POINT('Ctrl Pts',(86.4984319147047,-0.333919191023641,
340.90940950653));
#14457=CARTESIAN_POINT('Ctrl Pts',(86.4910183571245,-0.176851947027658,
340.914106352724));
#14458=CARTESIAN_POINT('Ctrl Pts',(86.4835942449878,-0.0195610890550666,
340.918809885739));
#14459=CARTESIAN_POINT('Ctrl Pts',(86.4761701328511,0.137738370374983,340.917228841115));
#14460=CARTESIAN_POINT('Ctrl Pts',(86.4687460207144,0.294510209793697,340.909415732442));
#14461=CARTESIAN_POINT('Ctrl Pts',(86.4648888955599,0.375959492104575,340.905356507925));
#14462=CARTESIAN_POINT('Ctrl Pts',(86.4610317704055,0.457266479000304,340.899615962269));
#14463=CARTESIAN_POINT('Ctrl Pts',(86.457174645251,0.538357036472173,340.892206909451));
#14464=CARTESIAN_POINT('Ctrl Pts',(86.449750667813,0.69443557813221,340.877946381531));
#14465=CARTESIAN_POINT('Ctrl Pts',(86.4423266903751,0.850182560432624,340.857458516544));
#14466=CARTESIAN_POINT('Ctrl Pts',(86.4349027129371,1.00506115637499,340.830761754218));
#14467=CARTESIAN_POINT('Ctrl Pts',(86.4274874969094,1.15975697227141,340.804096498087));
#14468=CARTESIAN_POINT('Ctrl Pts',(86.4200722808818,1.31358607753257,340.771236992768));
#14469=CARTESIAN_POINT('Ctrl Pts',(86.4126570648542,1.46601487947295,340.732253565193));
#14470=CARTESIAN_POINT('Ctrl Pts',(86.4052489837101,1.6182970151876,340.693307647275));
#14471=CARTESIAN_POINT('Ctrl Pts',(86.397840902566,1.76918117077637,340.648249629638));
#14472=CARTESIAN_POINT('Ctrl Pts',(86.3904328214219,1.91814219674899,340.597201182337));
#14473=CARTESIAN_POINT('Ctrl Pts',(86.3830302542479,2.06699234830908,340.546190731328));
#14474=CARTESIAN_POINT('Ctrl Pts',(86.3756276870739,2.21392186887688,340.48919884922));
#14475=CARTESIAN_POINT('Ctrl Pts',(86.3682251198999,2.35841917847937,340.426397473562));
#14476=CARTESIAN_POINT('Ctrl Pts',(86.3608264501452,2.50284041088029,340.363629162554));
#14477=CARTESIAN_POINT('Ctrl Pts',(86.3534277803904,2.64483164118487,340.295057597912));
#14478=CARTESIAN_POINT('Ctrl Pts',(86.3460291106357,2.78389984826712,340.220903389004));
#14479=CARTESIAN_POINT('Ctrl Pts',(86.3386316614317,2.92294511341351,340.146761413239));
#14480=CARTESIAN_POINT('Ctrl Pts',(86.3312342122277,3.0590679833657,340.06703879645));
#14481=CARTESIAN_POINT('Ctrl Pts',(86.3238367630237,3.19179859453153,339.982002839667));
#14482=CARTESIAN_POINT('Ctrl Pts',(86.3164396345602,3.32452345072947,339.896970569894));
#14483=CARTESIAN_POINT('Ctrl Pts',(86.3090425060968,3.45385602633921,339.80662561952));
#14484=CARTESIAN_POINT('Ctrl Pts',(86.3016453776333,3.57935432915095,339.711279353731));
#14485=CARTESIAN_POINT('Ctrl Pts',(86.2942471101967,3.70487195556828,339.615918406996));
#14486=CARTESIAN_POINT('Ctrl Pts',(86.2868488427601,3.82655383646696,339.515554837309));
#14487=CARTESIAN_POINT('Ctrl Pts',(86.2794505753235,3.94399015971994,339.410541030592));
#14488=CARTESIAN_POINT('Ctrl Pts',(86.2720497087978,4.0614677395886,339.30549033142));
#14489=CARTESIAN_POINT('Ctrl Pts',(86.264648842272,4.17469651419082,339.195786391189));
#14490=CARTESIAN_POINT('Ctrl Pts',(86.2572479757462,4.28330282048432,339.08181914231));
#14491=CARTESIAN_POINT('Ctrl Pts',(86.2498389823614,4.39202838688538,338.967726746497));
#14492=CARTESIAN_POINT('Ctrl Pts',(86.2424299889767,4.49612109048732,338.849361963128));
#14493=CARTESIAN_POINT('Ctrl Pts',(86.2350209955919,4.59524646433407,338.727149110852));
#14494=CARTESIAN_POINT('Ctrl Pts',(86.2276074380116,4.6944329028301,338.604860971244));
#14495=CARTESIAN_POINT('Ctrl Pts',(86.2201938804314,4.78864569121504,338.478720337424));
#14496=CARTESIAN_POINT('Ctrl Pts',(86.2127803228512,4.87759346762527,338.349180874047));
#14497=CARTESIAN_POINT('Ctrl Pts',(86.2053562107145,4.96666787747923,338.219456987528));
#14498=CARTESIAN_POINT('Ctrl Pts',(86.1979320985778,5.05046210666401,338.086324922291));
#14499=CARTESIAN_POINT('Ctrl Pts',(86.1905079864411,5.12873013477052,337.950264016524));
#14500=CARTESIAN_POINT('Ctrl Pts',(86.1866508612864,5.16939352649414,337.879574898077));
#14501=CARTESIAN_POINT('Ctrl Pts',(86.1827937361318,5.20856605518826,337.808095579537));
#14502=CARTESIAN_POINT('Ctrl Pts',(86.1789366109771,5.24621837823364,337.735895336153));
#14503=CARTESIAN_POINT('Ctrl Pts',(86.1715126335392,5.31868945074736,337.596928370755));
#14504=CARTESIAN_POINT('Ctrl Pts',(86.1640886561012,5.3857443968736,337.454870251285));
#14505=CARTESIAN_POINT('Ctrl Pts',(86.1566646786632,5.44710821507903,337.310182385813));
#14506=CARTESIAN_POINT('Ctrl Pts',(86.1492494626356,5.50839961474629,337.165665273791));
#14507=CARTESIAN_POINT('Ctrl Pts',(86.1418342466079,5.56401311126594,337.018524933571));
#14508=CARTESIAN_POINT('Ctrl Pts',(86.1344190305803,5.61371908643525,336.869248132564));
#14509=CARTESIAN_POINT('Ctrl Pts',(86.1270109494362,5.66337723476544,336.720114964943));
#14510=CARTESIAN_POINT('Ctrl Pts',(86.1196028682921,5.70713906078391,336.568849780765));
#14511=CARTESIAN_POINT('Ctrl Pts',(86.112194787148,5.74482269091336,336.415960032087));
#14512=CARTESIAN_POINT('Ctrl Pts',(86.1047922199741,5.78247827242856,336.263184082042));
#14513=CARTESIAN_POINT('Ctrl Pts',(86.0973896528001,5.81406457728902,336.108786335991));
#14514=CARTESIAN_POINT('Ctrl Pts',(86.0899870856261,5.83944934616971,335.953290037721));
#14515=CARTESIAN_POINT('Ctrl Pts',(86.0825884158713,5.86482075008083,335.797875607571));
#14516=CARTESIAN_POINT('Ctrl Pts',(86.0751897461165,5.88399706063643,335.641364144494));
#14517=CARTESIAN_POINT('Ctrl Pts',(86.0677910763617,5.89689699093968,335.48428962486));
#14518=CARTESIAN_POINT('Ctrl Pts',(86.0603936271578,5.90979479315489,335.327241017645));
#14519=CARTESIAN_POINT('Ctrl Pts',(86.0529961779538,5.91641823955004,335.169629909822));
#14520=CARTESIAN_POINT('Ctrl Pts',(86.0455987287498,5.91673783911079,335.011996071631));
#14521=CARTESIAN_POINT('Ctrl Pts',(86.0382016002864,5.91705742481426,334.854369068169));
#14522=CARTESIAN_POINT('Ctrl Pts',(86.0308044718229,5.91107370638444,334.696719709511));
#14523=CARTESIAN_POINT('Ctrl Pts',(86.0234073433595,5.8988093301012,334.539588173902));
#14524=CARTESIAN_POINT('Ctrl Pts',(86.0160090759229,5.88654306541016,334.382432443959));
#14525=CARTESIAN_POINT('Ctrl Pts',(86.0086108084863,5.86799424635611,334.225795067923));
#14526=CARTESIAN_POINT('Ctrl Pts',(86.0012125410497,5.8432374289237,334.0702113618));
#14527=CARTESIAN_POINT('Ctrl Pts',(85.9938116745239,5.81847191416096,333.914572997485));
#14528=CARTESIAN_POINT('Ctrl Pts',(85.9864108079982,5.78749411739314,333.759989408423));
#14529=CARTESIAN_POINT('Ctrl Pts',(85.9790099414724,5.75042973059065,333.60698583064));
#14530=CARTESIAN_POINT('Ctrl Pts',(85.9716009480876,5.71332464354791,333.4538142403));
#14531=CARTESIAN_POINT('Ctrl Pts',(85.9641919547029,5.67011970676866,333.30222648907));
#14532=CARTESIAN_POINT('Ctrl Pts',(85.9567829613181,5.62099073959442,333.152733460517));
#14533=CARTESIAN_POINT('Ctrl Pts',(85.9493694037379,5.57183150728205,333.003148339102));
#14534=CARTESIAN_POINT('Ctrl Pts',(85.9419558461577,5.51674110293494,332.855660860501));
#14535=CARTESIAN_POINT('Ctrl Pts',(85.9345422885775,5.45594335021597,332.710761541094));
#14536=CARTESIAN_POINT('Ctrl Pts',(85.9271181764409,5.39505904076532,332.565655930978));
#14537=CARTESIAN_POINT('Ctrl Pts',(85.9196940643042,5.32845131238363,332.42314617637));
#14538=CARTESIAN_POINT('Ctrl Pts',(85.9122699521675,5.25639011501967,332.283698558476));
#14539=CARTESIAN_POINT('Ctrl Pts',(85.9084128270127,5.21895142175617,332.211249906725));
#14540=CARTESIAN_POINT('Ctrl Pts',(85.9045557018579,5.18004144084578,332.139627330889));
#14541=CARTESIAN_POINT('Ctrl Pts',(85.900698576703,5.1397025483473,332.068892994616));
#14542=CARTESIAN_POINT('Ctrl Pts',(85.893274599265,5.06206051814006,331.932747524736));
#14543=CARTESIAN_POINT('Ctrl Pts',(85.885850621827,4.97888809376132,331.799483790245));
#14544=CARTESIAN_POINT('Ctrl Pts',(85.878426644389,4.89042446399098,331.669582740181));
#14545=CARTESIAN_POINT('Ctrl Pts',(85.8710114283614,4.80206523461385,331.539834992901));
#14546=CARTESIAN_POINT('Ctrl Pts',(85.8635962123337,4.70842743748956,331.413442336211));
#14547=CARTESIAN_POINT('Ctrl Pts',(85.8561809963061,4.60979614613365,331.290861278734));
#14548=CARTESIAN_POINT('Ctrl Pts',(85.848772915162,4.51125975731002,331.168398168134));
#14549=CARTESIAN_POINT('Ctrl Pts',(85.8413648340179,4.40773967194467,331.049739644264));
#14550=CARTESIAN_POINT('Ctrl Pts',(85.8339567528738,4.29956419507076,330.935313259922));
#14551=CARTESIAN_POINT('Ctrl Pts',(85.8265541856997,4.19146923517896,330.820972045226));
#14552=CARTESIAN_POINT('Ctrl Pts',(85.8191516185257,4.07872603857352,330.710856967875));
#14553=CARTESIAN_POINT('Ctrl Pts',(85.8117490513516,3.96170303900783,330.605362404792));
#14554=CARTESIAN_POINT('Ctrl Pts',(85.8043503815968,3.84474165154055,330.499923384136));
#14555=CARTESIAN_POINT('Ctrl Pts',(85.7969517118421,3.72350522519156,330.399100282185));
#14556=CARTESIAN_POINT('Ctrl Pts',(85.7895530420873,3.59839880307863,330.303250420078));
#14557=CARTESIAN_POINT('Ctrl Pts',(85.7821555928833,3.47331301964068,330.207416370221));
#14558=CARTESIAN_POINT('Ctrl Pts',(85.7747581436793,3.34435880348351,330.116554158676));
#14559=CARTESIAN_POINT('Ctrl Pts',(85.7673606944754,3.21197409963915,330.030980685714));
#14560=CARTESIAN_POINT('Ctrl Pts',(85.7599635660119,3.07959513576494,329.945410923069));
#14561=CARTESIAN_POINT('Ctrl Pts',(85.7525664375484,2.94378629337883,329.865129645665));
#14562=CARTESIAN_POINT('Ctrl Pts',(85.7451693090849,2.80501407509356,329.790410131207));
#14563=CARTESIAN_POINT('Ctrl Pts',(85.7377710416483,2.6662204893507,329.715679111809));
#14564=CARTESIAN_POINT('Ctrl Pts',(85.7303727742117,2.52446294780906,329.64651173745));
#14565=CARTESIAN_POINT('Ctrl Pts',(85.7229745067751,2.38023195563828,329.583135002618));
#14566=CARTESIAN_POINT('Ctrl Pts',(85.7155736402494,2.23595029360381,329.519736002873));
#14567=CARTESIAN_POINT('Ctrl Pts',(85.7081727737236,2.08919379232855,329.462131843012));
#14568=CARTESIAN_POINT('Ctrl Pts',(85.7007719071979,1.94047215312956,329.410501061327));
#14569=CARTESIAN_POINT('Ctrl Pts',(85.6933629138131,1.79158720335175,329.358813584107));
#14570=CARTESIAN_POINT('Ctrl Pts',(85.6859539204284,1.64073315896957,329.313112706888));
#14571=CARTESIAN_POINT('Ctrl Pts',(85.6785449270436,1.48843477880754,329.273527047847));
#14572=CARTESIAN_POINT('Ctrl Pts',(85.6711313694633,1.33604257758979,329.233917002675));
#14573=CARTESIAN_POINT('Ctrl Pts',(85.663717811883,1.18220463144588,329.200429761492));
#14574=CARTESIAN_POINT('Ctrl Pts',(85.6563042543028,1.02745454989345,329.173142552765));
#14575=CARTESIAN_POINT('Ctrl Pts',(85.6488801421661,0.872484153269253,329.1458164957));
#14576=CARTESIAN_POINT('Ctrl Pts',(85.6414560300294,0.71659939652762,329.124708150083));
#14577=CARTESIAN_POINT('Ctrl Pts',(85.6340319178927,0.560338470891678,329.109842840761));
#14578=CARTESIAN_POINT('Ctrl Pts',(85.6301747927382,0.479154628859491,329.102119714081));
#14579=CARTESIAN_POINT('Ctrl Pts',(85.6263176675837,0.397869253520564,329.09608086165));
#14580=CARTESIAN_POINT('Ctrl Pts',(85.6224605424292,0.316557551728029,329.091724288852));
#14581=CARTESIAN_POINT('Ctrl Pts',(85.6150365649912,0.160053363926919,329.083339002696));
#14582=CARTESIAN_POINT('Ctrl Pts',(85.6076125875532,0.00297967527304754,
329.081163815357));
#14583=CARTESIAN_POINT('Ctrl Pts',(85.6001886101152,-0.154129635153365,
329.08525785701));
#14584=CARTESIAN_POINT('Ctrl Pts',(85.5927733940876,-0.311053532954991,
329.089347067077));
#14585=CARTESIAN_POINT('Ctrl Pts',(85.58535817806,-0.468012599393245,329.099690769409));
#14586=CARTESIAN_POINT('Ctrl Pts',(85.5779429620324,-0.624468676991852,
329.116296282616));
#14587=CARTESIAN_POINT('Ctrl Pts',(85.5705348808883,-0.780774213340468,
329.132885818082));
#14588=CARTESIAN_POINT('Ctrl Pts',(85.5631267997443,-0.936577355703673,
329.155725130479));
#14589=CARTESIAN_POINT('Ctrl Pts',(85.5557187186002,-1.09134090112104,329.184769514453));
#14590=CARTESIAN_POINT('Ctrl Pts',(85.5483161514262,-1.2459892532048,329.213792280161));
#14591=CARTESIAN_POINT('Ctrl Pts',(85.5409135842522,-1.39959918383672,329.249010852699));
#14592=CARTESIAN_POINT('Ctrl Pts',(85.5335110170782,-1.5516396724024,329.290328828249));
#14593=CARTESIAN_POINT('Ctrl Pts',(85.5261123473235,-1.70360011231513,329.331625050065));
#14594=CARTESIAN_POINT('Ctrl Pts',(85.5187136775688,-1.85399239655353,329.379014181752));
#14595=CARTESIAN_POINT('Ctrl Pts',(85.5113150078141,-2.00229685407605,329.432348980885));
#14596=CARTESIAN_POINT('Ctrl Pts',(85.5039175586101,-2.15057684596881,329.485674981431));
#14597=CARTESIAN_POINT('Ctrl Pts',(85.4965201094061,-2.29676934387149,329.544944576575));
#14598=CARTESIAN_POINT('Ctrl Pts',(85.4891226602022,-2.44037086239749,329.609960981917));
#14599=CARTESIAN_POINT('Ctrl Pts',(85.4817255317387,-2.583966154612,329.67497456826));
#14600=CARTESIAN_POINT('Ctrl Pts',(85.4743284032753,-2.72497035083156,329.745734315435));
#14601=CARTESIAN_POINT('Ctrl Pts',(85.4669312748118,-2.86290119467269,329.821995817688));
#14602=CARTESIAN_POINT('Ctrl Pts',(85.4595330073752,-3.00085327642105,329.898269062309));
#14603=CARTESIAN_POINT('Ctrl Pts',(85.4521347399386,-3.13573073691531,329.980045568166));
#14604=CARTESIAN_POINT('Ctrl Pts',(85.4447364725019,-3.26707725115514,330.067035698742));
#14605=CARTESIAN_POINT('Ctrl Pts',(85.4373356059762,-3.39846990880614,330.154056389865));
#14606=CARTESIAN_POINT('Ctrl Pts',(85.4299347394505,-3.52632883949095,330.246294146473));
#14607=CARTESIAN_POINT('Ctrl Pts',(85.4225338729247,-3.65022807792137,330.343416967168));
#14608=CARTESIAN_POINT('Ctrl Pts',(85.41512487954,-3.7742633695609,330.440646438007));
#14609=CARTESIAN_POINT('Ctrl Pts',(85.4077158861552,-3.89432999161803,330.542771455278));
#14610=CARTESIAN_POINT('Ctrl Pts',(85.4003068927705,-4.0100358092131,330.649420340767));
#14611=CARTESIAN_POINT('Ctrl Pts',(85.3928933351902,-4.12581290558276,330.756134925649));
#14612=CARTESIAN_POINT('Ctrl Pts',(85.3854797776101,-4.23722358099036,330.867378668847));
#14613=CARTESIAN_POINT('Ctrl Pts',(85.3780662200298,-4.34391412564184,330.98274463949));
#14614=CARTESIAN_POINT('Ctrl Pts',(85.3706421078932,-4.45075656381594,331.098274854712));
#14615=CARTESIAN_POINT('Ctrl Pts',(85.3632179957565,-4.55286520851005,331.217938735301));
#14616=CARTESIAN_POINT('Ctrl Pts',(85.3557938836198,-4.64992751736846,331.341297409502));
#14617=CARTESIAN_POINT('Ctrl Pts',(85.351936758465,-4.7003552946154,331.405387207254));
#14618=CARTESIAN_POINT('Ctrl Pts',(85.3480796333101,-4.74942167521198,331.47047384397));
#14619=CARTESIAN_POINT('Ctrl Pts',(85.3442225081553,-4.79708763772977,331.536492997201));
#14620=CARTESIAN_POINT('Ctrl Pts',(85.3367393826128,-4.88956334627111,331.66457533625));
#14621=CARTESIAN_POINT('Ctrl Pts',(85.3292562570703,-4.97704343511309,331.796554376371));
#14622=CARTESIAN_POINT('Ctrl Pts',(85.3217731315277,-5.05918476797303,331.932007163305));
#14623=CARTESIAN_POINT('Ctrl Pts',(85.3142990850663,-5.14122644089619,332.067295608906));
#14624=CARTESIAN_POINT('Ctrl Pts',(85.3068250386048,-5.21794206427955,332.206049102698));
#14625=CARTESIAN_POINT('Ctrl Pts',(85.2993509921433,-5.28902964290597,332.347812978133));
#14626=CARTESIAN_POINT('Ctrl Pts',(85.2918846182601,-5.3600442456667,332.489431324043));
#14627=CARTESIAN_POINT('Ctrl Pts',(85.2844182443769,-5.4254421437923,332.63405357482));
#14628=CARTESIAN_POINT('Ctrl Pts',(85.2769518704937,-5.48496547831313,332.781197560797));
#14629=CARTESIAN_POINT('Ctrl Pts',(85.2694917677292,-5.54443881829795,332.928217958347));
#14630=CARTESIAN_POINT('Ctrl Pts',(85.2620316649647,-5.59804728371563,333.077755536417));
#14631=CARTESIAN_POINT('Ctrl Pts',(85.2545715622002,-5.64557970362559,333.229305115919));
#14632=CARTESIAN_POINT('Ctrl Pts',(85.2471167580928,-5.6930783628758,333.380747054913));
#14633=CARTESIAN_POINT('Ctrl Pts',(85.2396619539853,-5.73450946622863,333.534197800506));
#14634=CARTESIAN_POINT('Ctrl Pts',(85.2322071498779,-5.76971063860679,333.689133985013));
#14635=CARTESIAN_POINT('Ctrl Pts',(85.2247555166807,-5.80489683812204,333.844004267219));
#14636=CARTESIAN_POINT('Ctrl Pts',(85.2173038834836,-5.83385830372132,334.000358374298));
#14637=CARTESIAN_POINT('Ctrl Pts',(85.2098522502864,-5.85648299479626,334.157659514114));
#14638=CARTESIAN_POINT('Ctrl Pts',(85.2024015160298,-5.87910495650304,334.314941677639));
#14639=CARTESIAN_POINT('Ctrl Pts',(85.1949507817731,-5.89539160873179,334.473170285755));
#14640=CARTESIAN_POINT('Ctrl Pts',(85.1875000475164,-5.90528232234687,334.631799978439));
#14641=CARTESIAN_POINT('Ctrl Pts',(85.1816840332455,-5.91300297504414,334.755625701471));
#14642=CARTESIAN_POINT('Ctrl Pts',(85.1758680189745,-5.91682740891254,334.87969558763));
#14643=CARTESIAN_POINT('Ctrl Pts',(85.1700520047035,-5.91674881247257,335.003748680365));
#14644=CARTESIAN_POINT('',(83.4200520047036,-5.92472559629233,335.002923715034));
#14645=CARTESIAN_POINT('Ctrl Pts',(85.1700498850932,-5.90944875995897,335.003789209877));
#14646=CARTESIAN_POINT('Ctrl Pts',(85.1353614146893,-5.91370990462514,335.742769459017));
#14647=CARTESIAN_POINT('Ctrl Pts',(85.0079269328602,-5.44210307607092,338.452296737771));
#14648=CARTESIAN_POINT('Ctrl Pts',(84.7877464396077,-1.37745943898813,341.859681363963));
#14649=CARTESIAN_POINT('Ctrl Pts',(84.5095084053333,5.02303006280172,339.870502223532));
#14650=CARTESIAN_POINT('Ctrl Pts',(84.2312703710595,6.81395901576062,333.411735081052));
#14651=CARTESIAN_POINT('Ctrl Pts',(83.9530323367856,2.35181835382513,328.410495211943));
#14652=CARTESIAN_POINT('Ctrl Pts',(83.6826262146669,-4.08219951646664,329.426907744826));
#14653=CARTESIAN_POINT('Ctrl Pts',(83.5049661039729,-5.91383814749851,333.205903189172));
#14654=CARTESIAN_POINT('Ctrl Pts',(83.4200520047036,-5.92472559629233,335.002923715034));
#14655=CARTESIAN_POINT('',(81.6700520047036,-5.91801367655859,334.994687890905));
#14656=CARTESIAN_POINT('Ctrl Pts',(83.4200520047036,-5.92472559629233,335.002923715034));
#14657=CARTESIAN_POINT('Ctrl Pts',(83.4122200925483,-5.92572978220824,335.168668944872));
#14658=CARTESIAN_POINT('Ctrl Pts',(83.404388180393,-5.91937917051338,335.334336070522));
#14659=CARTESIAN_POINT('Ctrl Pts',(83.303810256813,-5.74017621052549,337.453586964006));
#14660=CARTESIAN_POINT('Ctrl Pts',(83.1183182339638,-3.27705977547671,341.181707057858));
#14661=CARTESIAN_POINT('Ctrl Pts',(82.8400801996897,3.42492426372844,341.101025873486));
#14662=CARTESIAN_POINT('Ctrl Pts',(82.5618421654159,6.98390585790928,335.42152329601));
#14663=CARTESIAN_POINT('Ctrl Pts',(82.2836041311419,4.13386012856826,329.35519501146));
#14664=CARTESIAN_POINT('Ctrl Pts',(82.0053660968678,-2.50976802508626,328.469020947708));
#14665=CARTESIAN_POINT('Ctrl Pts',(81.8008487213886,-5.70019332344303,332.223047555137));
#14666=CARTESIAN_POINT('Ctrl Pts',(81.6890773573338,-5.92214175837517,334.590937491054));
#14667=CARTESIAN_POINT('Ctrl Pts',(81.6700520047036,-5.9184019942076,334.994687542344));
#14668=CARTESIAN_POINT('',(79.9200520047356,-5.91674999747214,334.99982704509));
#14669=CARTESIAN_POINT('Ctrl Pts',(81.6700520047036,-5.91674761639107,334.994689027342));
#14670=CARTESIAN_POINT('Ctrl Pts',(81.662747770902,-5.91688671416704,335.149652437497));
#14671=CARTESIAN_POINT('Ctrl Pts',(81.6554435371003,-5.91093377111608,335.304809948067));
#14672=CARTESIAN_POINT('Ctrl Pts',(81.6481393032986,-5.89886984741152,335.459635818664));
#14673=CARTESIAN_POINT('Ctrl Pts',(81.6408408138345,-5.88681541125234,335.614339928091));
#14674=CARTESIAN_POINT('Ctrl Pts',(81.6335423243703,-5.86865958823044,335.768712534865));
#14675=CARTESIAN_POINT('Ctrl Pts',(81.6262438349062,-5.84443550203431,335.922227859621));
#14676=CARTESIAN_POINT('Ctrl Pts',(81.6188540929651,-5.81990854387023,336.077662575191));
#14677=CARTESIAN_POINT('Ctrl Pts',(81.6114643510241,-5.7891605465858,336.232218026418));
#14678=CARTESIAN_POINT('Ctrl Pts',(81.604074609083,-5.75228016881055,336.385353175912));
#14679=CARTESIAN_POINT('Ctrl Pts',(81.5967815438203,-5.71588228047122,336.536484926949));
#14680=CARTESIAN_POINT('Ctrl Pts',(81.5894884785576,-5.67351160277635,336.686232932781));
#14681=CARTESIAN_POINT('Ctrl Pts',(81.5821954132949,-5.62530478166383,336.834087423186));
#14682=CARTESIAN_POINT('Ctrl Pts',(81.5749026303751,-5.57709982682531,336.981936189567));
#14683=CARTESIAN_POINT('Ctrl Pts',(81.5676098474554,-5.52305929713086,337.127891220378));
#14684=CARTESIAN_POINT('Ctrl Pts',(81.5603170645357,-5.46336948475028,337.271458658131));
#14685=CARTESIAN_POINT('Ctrl Pts',(81.5530230288349,-5.40366941863425,337.415050758427));
#14686=CARTESIAN_POINT('Ctrl Pts',(81.5457289931341,-5.33831828692846,337.556254094363));
#14687=CARTESIAN_POINT('Ctrl Pts',(81.5384349574334,-5.26755009681816,337.694595802715));
#14688=CARTESIAN_POINT('Ctrl Pts',(81.5309728800073,-5.19515153235098,337.836124660173));
#14689=CARTESIAN_POINT('Ctrl Pts',(81.5235108025811,-5.11708346993486,337.974658054906));
#14690=CARTESIAN_POINT('Ctrl Pts',(81.516048725155,-5.03364509571469,338.109718252975));
#14691=CARTESIAN_POINT('Ctrl Pts',(81.5087438989445,-4.95196505031146,338.241932275763));
#14692=CARTESIAN_POINT('Ctrl Pts',(81.501439072734,-4.86513904868359,338.370817744346));
#14693=CARTESIAN_POINT('Ctrl Pts',(81.4941342465235,-4.77349003294312,338.495958161634));
#14694=CARTESIAN_POINT('Ctrl Pts',(81.4865935434896,-4.67888162048663,338.625139431264));
#14695=CARTESIAN_POINT('Ctrl Pts',(81.4790528404557,-4.57913377475567,338.750329374966));
#14696=CARTESIAN_POINT('Ctrl Pts',(81.4715121374218,-4.47464411467867,338.871109738753));
#14697=CARTESIAN_POINT('Ctrl Pts',(81.4639714343879,-4.37015445460175,338.991890102541));
#14698=CARTESIAN_POINT('Ctrl Pts',(81.4564307313539,-4.2609233356176,339.108260612671));
#14699=CARTESIAN_POINT('Ctrl Pts',(81.44889002832,-4.14738639006992,339.219847946782));
#14700=CARTESIAN_POINT('Ctrl Pts',(81.441466050882,-4.03560692887947,339.329707975361));
#14701=CARTESIAN_POINT('Ctrl Pts',(81.434042073444,-3.91929070850586,339.435289280455));
#14702=CARTESIAN_POINT('Ctrl Pts',(81.426618096006,-3.79879883789278,339.536194214507));
#14703=CARTESIAN_POINT('Ctrl Pts',(81.4192028799784,-3.67844916581601,339.636980065554));
#14704=CARTESIAN_POINT('Ctrl Pts',(81.4117876639508,-3.55393393590162,339.733100293574));
#14705=CARTESIAN_POINT('Ctrl Pts',(81.4043724479231,-3.42565175318212,339.824193261927));
#14706=CARTESIAN_POINT('Ctrl Pts',(81.396964366779,-3.29749300293311,339.915198581084));
#14707=CARTESIAN_POINT('Ctrl Pts',(81.3895562856349,-3.16557481793074,340.001186055908));
#14708=CARTESIAN_POINT('Ctrl Pts',(81.3821482044908,-3.0303295168267,340.081833683027));
#14709=CARTESIAN_POINT('Ctrl Pts',(81.3747456373168,-2.89518488126986,340.162421282644));
#14710=CARTESIAN_POINT('Ctrl Pts',(81.3673430701428,-2.75671837972484,340.23767675813));
#14711=CARTESIAN_POINT('Ctrl Pts',(81.3599405029688,-2.61539190982473,340.307320955108));
#14712=CARTESIAN_POINT('Ctrl Pts',(81.3525418332141,-2.47413984769425,340.376928484719));
#14713=CARTESIAN_POINT('Ctrl Pts',(81.3451431634593,-2.33003114994793,340.440930454958));
#14714=CARTESIAN_POINT('Ctrl Pts',(81.3377444937046,-2.1835528503593,340.499093335468));
#14715=CARTESIAN_POINT('Ctrl Pts',(81.3303470445007,-2.03709871514119,340.557246620909));
#14716=CARTESIAN_POINT('Ctrl Pts',(81.3229495952967,-1.88827610044171,340.609562590799));
#14717=CARTESIAN_POINT('Ctrl Pts',(81.3155521460927,-1.73759269253072,340.65585556723));
#14718=CARTESIAN_POINT('Ctrl Pts',(81.3081550176293,-1.58691581798949,340.702146536478));
#14719=CARTESIAN_POINT('Ctrl Pts',(81.3007578891658,-1.43437866741149,340.742414921911));
#14720=CARTESIAN_POINT('Ctrl Pts',(81.2933607607023,-1.28050452758628,340.776524795873));
#14721=CARTESIAN_POINT('Ctrl Pts',(81.2859624932657,-1.12660669498486,340.810639921903));
#14722=CARTESIAN_POINT('Ctrl Pts',(81.2785642258291,-0.971371827624401,
340.838594567584));
#14723=CARTESIAN_POINT('Ctrl Pts',(81.2711659583925,-0.815333705432265,
340.860303875337));
#14724=CARTESIAN_POINT('Ctrl Pts',(81.2637650918667,-0.659240765406648,
340.882020809798));
#14725=CARTESIAN_POINT('Ctrl Pts',(81.256364225341,-0.50234437812377,340.89748798658));
#14726=CARTESIAN_POINT('Ctrl Pts',(81.2489633588152,-0.345183600167206,
340.906672400318));
#14727=CARTESIAN_POINT('Ctrl Pts',(81.2415543654305,-0.187850244651283,
340.91586689942));
#14728=CARTESIAN_POINT('Ctrl Pts',(81.2341453720458,-0.0302522914625299,
340.918764835873));
#14729=CARTESIAN_POINT('Ctrl Pts',(81.226736378661,0.127070307032321,340.915385338215));
#14730=CARTESIAN_POINT('Ctrl Pts',(81.2193228210808,0.284489821674369,340.91200375867));
#14731=CARTESIAN_POINT('Ctrl Pts',(81.2119092635005,0.441633271979515,340.902337062137));
#14732=CARTESIAN_POINT('Ctrl Pts',(81.2044957059203,0.597966182245034,340.88645623507));
#14733=CARTESIAN_POINT('Ctrl Pts',(81.1970715937836,0.754521661028995,340.870552798737));
#14734=CARTESIAN_POINT('Ctrl Pts',(81.189647481647,0.910263926598655,340.848417615111));
#14735=CARTESIAN_POINT('Ctrl Pts',(81.1822233695103,1.06466822753262,340.820172860645));
#14736=CARTESIAN_POINT('Ctrl Pts',(81.1783662443556,1.14488747828769,340.805498573547));
#14737=CARTESIAN_POINT('Ctrl Pts',(81.1745091192008,1.22474581389733,340.789176005825));
#14738=CARTESIAN_POINT('Ctrl Pts',(81.1706519940461,1.3041714123094,340.771227554846));
#14739=CARTESIAN_POINT('Ctrl Pts',(81.1632280166081,1.45704533445618,340.736681386452));
#14740=CARTESIAN_POINT('Ctrl Pts',(81.1558040391702,1.6087762874556,340.696004697682));
#14741=CARTESIAN_POINT('Ctrl Pts',(81.1483800617322,1.75883446422273,340.649285962842));
#14742=CARTESIAN_POINT('Ctrl Pts',(81.1409648457046,1.9087155497638,340.602622363138));
#14743=CARTESIAN_POINT('Ctrl Pts',(81.133549629677,2.05692743572992,340.549931020646));
#14744=CARTESIAN_POINT('Ctrl Pts',(81.1261344136493,2.2029503061003,340.491351428506));
#14745=CARTESIAN_POINT('Ctrl Pts',(81.1187263325052,2.34883267400025,340.432828201354));
#14746=CARTESIAN_POINT('Ctrl Pts',(81.1113182513611,2.49252987541165,340.368428141822));
#14747=CARTESIAN_POINT('Ctrl Pts',(81.103910170217,2.63353717839881,340.298340541386));
#14748=CARTESIAN_POINT('Ctrl Pts',(81.0965076030431,2.77443952707464,340.22830510843));
#14749=CARTESIAN_POINT('Ctrl Pts',(81.089105035869,2.91265563110731,340.152590729172));
#14750=CARTESIAN_POINT('Ctrl Pts',(81.081702468695,3.04770078431308,340.071434756733));
#14751=CARTESIAN_POINT('Ctrl Pts',(81.0743037989403,3.18267483683686,339.990321512558));
#14752=CARTESIAN_POINT('Ctrl Pts',(81.0669051291855,3.31448094433997,339.903772572727));
#14753=CARTESIAN_POINT('Ctrl Pts',(81.0595064594307,3.44265916424283,339.812071117653));
#14754=CARTESIAN_POINT('Ctrl Pts',(81.0521090102268,3.570816238719,339.720384790473));
#14755=CARTESIAN_POINT('Ctrl Pts',(81.0447115610228,3.69534631016562,339.623547851978));
#14756=CARTESIAN_POINT('Ctrl Pts',(81.0373141118188,3.81581849989679,339.521886745413));
#14757=CARTESIAN_POINT('Ctrl Pts',(81.0299169833553,3.93628546616384,339.420230046697));
#14758=CARTESIAN_POINT('Ctrl Pts',(81.0225198548918,4.05269461532006,339.313749836495));
#14759=CARTESIAN_POINT('Ctrl Pts',(81.0151227264284,4.16464846239253,339.20281259958));
#14760=CARTESIAN_POINT('Ctrl Pts',(81.0077244589917,4.27661954756302,339.0918582811));
#14761=CARTESIAN_POINT('Ctrl Pts',(81.0003261915551,4.38413369960563,338.97644583216));
#14762=CARTESIAN_POINT('Ctrl Pts',(80.9929279241185,4.48683070102693,338.856978198386));
#14763=CARTESIAN_POINT('Ctrl Pts',(80.9855270575927,4.58956378098481,338.737468594375));
#14764=CARTESIAN_POINT('Ctrl Pts',(80.978126191067,4.68747609779013,338.613901251934));
#14765=CARTESIAN_POINT('Ctrl Pts',(80.9707253245412,4.78024818207935,338.486711614147));
#14766=CARTESIAN_POINT('Ctrl Pts',(80.9633163311564,4.87312213898621,338.359382309978));
#14767=CARTESIAN_POINT('Ctrl Pts',(80.9559073377717,4.96084437101275,338.228423068635));
#14768=CARTESIAN_POINT('Ctrl Pts',(80.9484983443869,5.04313876454832,338.094298299132));
#14769=CARTESIAN_POINT('Ctrl Pts',(80.9410847868067,5.12548385426883,337.960090904145));
#14770=CARTESIAN_POINT('Ctrl Pts',(80.9336712292265,5.20239426077343,337.822714420106));
#14771=CARTESIAN_POINT('Ctrl Pts',(80.9262576716462,5.27364044261458,337.682656713879));
#14772=CARTESIAN_POINT('Ctrl Pts',(80.9188335595096,5.34498805643899,337.542399609866));
#14773=CARTESIAN_POINT('Ctrl Pts',(80.9114094473729,5.41065518468264,337.399453998156));
#14774=CARTESIAN_POINT('Ctrl Pts',(80.9039853352362,5.47046059502883,337.254327270105));
#14775=CARTESIAN_POINT('Ctrl Pts',(80.9001282100816,5.5015319135085,337.178928091985));
#14776=CARTESIAN_POINT('Ctrl Pts',(80.896271084927,5.53102184575222,337.102940435887));
#14777=CARTESIAN_POINT('Ctrl Pts',(80.8924139597724,5.55891035915082,337.026436819007));
#14778=CARTESIAN_POINT('Ctrl Pts',(80.8849899823343,5.61258860031539,336.879186962474));
#14779=CARTESIAN_POINT('Ctrl Pts',(80.8775660048964,5.66049302991841,336.729580676738));
#14780=CARTESIAN_POINT('Ctrl Pts',(80.8701420274583,5.7024113388756,336.578111366401));
#14781=CARTESIAN_POINT('Ctrl Pts',(80.8627268114307,5.74428017792118,336.42682081264));
#14782=CARTESIAN_POINT('Ctrl Pts',(80.8553115954031,5.78017685979185,336.273671966918));
#14783=CARTESIAN_POINT('Ctrl Pts',(80.8478963793755,5.80993738496833,336.119177441359));
#14784=CARTESIAN_POINT('Ctrl Pts',(80.8404882982314,5.83966927471737,335.964831569655));
#14785=CARTESIAN_POINT('Ctrl Pts',(80.8330802170873,5.86327669176948,335.809142959855));
#14786=CARTESIAN_POINT('Ctrl Pts',(80.8256721359432,5.88064567595252,335.652638488293));
#14787=CARTESIAN_POINT('Ctrl Pts',(80.8182695687692,5.89800173208338,335.496250505867));
#14788=CARTESIAN_POINT('Ctrl Pts',(80.8108670015952,5.90912855999987,335.339048240168));
#14789=CARTESIAN_POINT('Ctrl Pts',(80.8034644344212,5.91396345267819,335.181567736359));
#14790=CARTESIAN_POINT('Ctrl Pts',(80.7960657646664,5.91879579980669,335.024170145347));
#14791=CARTESIAN_POINT('Ctrl Pts',(80.7886670949116,5.91734279766458,334.866494980067));
#14792=CARTESIAN_POINT('Ctrl Pts',(80.7812684251568,5.9095936773828,334.709082261219));
#14793=CARTESIAN_POINT('Ctrl Pts',(80.7738709759528,5.9018458354653,334.551695510584));
#14794=CARTESIAN_POINT('Ctrl Pts',(80.7664735267488,5.88780395515307,334.39457149285));
#14795=CARTESIAN_POINT('Ctrl Pts',(80.7590760775448,5.86750937635446,334.238249200268));
#14796=CARTESIAN_POINT('Ctrl Pts',(80.7516789490813,5.8472156774934,334.081933685548));
#14797=CARTESIAN_POINT('Ctrl Pts',(80.7442818206178,5.82066986724324,333.926420196969));
#14798=CARTESIAN_POINT('Ctrl Pts',(80.7368846921543,5.78796502854048,333.772241314064));
#14799=CARTESIAN_POINT('Ctrl Pts',(80.7294864247177,5.75525515410893,333.618038691458));
#14800=CARTESIAN_POINT('Ctrl Pts',(80.7220881572811,5.71638444040983,333.465171448806));
#14801=CARTESIAN_POINT('Ctrl Pts',(80.7146898898445,5.67149679866059,333.31416055768));
#14802=CARTESIAN_POINT('Ctrl Pts',(80.7072890233187,5.62659338741082,333.16309661484));
#14803=CARTESIAN_POINT('Ctrl Pts',(80.6998881567929,5.57566894578945,333.013890679483));
#14804=CARTESIAN_POINT('Ctrl Pts',(80.6924872902672,5.51891676397256,332.867047043453));
#14805=CARTESIAN_POINT('Ctrl Pts',(80.6850782968824,5.46210226283423,332.720042159071));
#14806=CARTESIAN_POINT('Ctrl Pts',(80.6776693034977,5.39944737614575,332.575405102757));
#14807=CARTESIAN_POINT('Ctrl Pts',(80.6702603101129,5.33119321443762,332.433619382704));
#14808=CARTESIAN_POINT('Ctrl Pts',(80.6628467525326,5.26289700581145,332.291746317755));
#14809=CARTESIAN_POINT('Ctrl Pts',(80.6554331949523,5.18899482366178,332.152728417939));
#14810=CARTESIAN_POINT('Ctrl Pts',(80.6480196373721,5.10977270759461,332.017022722309));
#14811=CARTESIAN_POINT('Ctrl Pts',(80.6405955252354,5.03043780434191,331.881123824777));
#14812=CARTESIAN_POINT('Ctrl Pts',(80.6331714130987,4.94576804091561,331.748546862977));
#14813=CARTESIAN_POINT('Ctrl Pts',(80.625747300962,4.85609201832578,331.619718817605));
#14814=CARTESIAN_POINT('Ctrl Pts',(80.6218901758074,4.80950171417569,331.552787461334));
#14815=CARTESIAN_POINT('Ctrl Pts',(80.6180330506528,4.76156076750666,331.486867467286));
#14816=CARTESIAN_POINT('Ctrl Pts',(80.6141759254982,4.71231931878221,331.422014924524));
#14817=CARTESIAN_POINT('Ctrl Pts',(80.6067519480602,4.61754214933732,331.297190399789));
#14818=CARTESIAN_POINT('Ctrl Pts',(80.5993279706223,4.51765886756541,331.175945997321));
#14819=CARTESIAN_POINT('Ctrl Pts',(80.5919039931843,4.41296949529584,331.0587272619));
#14820=CARTESIAN_POINT('Ctrl Pts',(80.5844887771566,4.30840367223699,330.941646862224));
#14821=CARTESIAN_POINT('Ctrl Pts',(80.577073561129,4.19904329489378,330.828582948518));
#14822=CARTESIAN_POINT('Ctrl Pts',(80.5696583451014,4.08523068018667,330.71995083531));
#14823=CARTESIAN_POINT('Ctrl Pts',(80.5622502639573,3.97152757540421,330.611423247375));
#14824=CARTESIAN_POINT('Ctrl Pts',(80.5548421828132,3.85338102991335,330.50731922656));
#14825=CARTESIAN_POINT('Ctrl Pts',(80.5474341016691,3.73117243487341,330.408019727423));
#14826=CARTESIAN_POINT('Ctrl Pts',(80.5400315344951,3.60905480192282,330.308794138716));
#14827=CARTESIAN_POINT('Ctrl Pts',(80.5326289673211,3.48288142797572,330.214366185506));
#14828=CARTESIAN_POINT('Ctrl Pts',(80.5252264001471,3.35306915047842,330.125078684265));
#14829=CARTESIAN_POINT('Ctrl Pts',(80.5178277303924,3.22332521857768,330.035838192503));
#14830=CARTESIAN_POINT('Ctrl Pts',(80.5104290606376,3.08994650541052,329.951732973671));
#14831=CARTESIAN_POINT('Ctrl Pts',(80.5030303908828,2.95338129825054,329.873064319728));
#14832=CARTESIAN_POINT('Ctrl Pts',(80.4956329416788,2.81683862010928,329.794408643671));
#14833=CARTESIAN_POINT('Ctrl Pts',(80.4882354924749,2.67711081434308,329.721187938625));
#14834=CARTESIAN_POINT('Ctrl Pts',(80.4808380432709,2.53467350243085,329.653659120616));
#14835=CARTESIAN_POINT('Ctrl Pts',(80.4734409148075,2.39224236635234,329.586133230538));
#14836=CARTESIAN_POINT('Ctrl Pts',(80.466043786344,2.24710229494725,329.524298896675));
#14837=CARTESIAN_POINT('Ctrl Pts',(80.4586466578805,2.09975151822453,329.468366052945));
#14838=CARTESIAN_POINT('Ctrl Pts',(80.4512483904439,1.95237805316047,329.412424596953));
#14839=CARTESIAN_POINT('Ctrl Pts',(80.4438501230074,1.80279355395116,329.362386572853));
#14840=CARTESIAN_POINT('Ctrl Pts',(80.4364518555708,1.65151399532478,329.318412890244));
#14841=CARTESIAN_POINT('Ctrl Pts',(80.429050989045,1.50018129059802,329.274423759218));
#14842=CARTESIAN_POINT('Ctrl Pts',(80.4216501225192,1.34715269898234,329.236503315546));
#14843=CARTESIAN_POINT('Ctrl Pts',(80.4142492559935,1.1929568906518,329.204761918649));
#14844=CARTESIAN_POINT('Ctrl Pts',(80.4068402626087,1.03859176058234,329.172985666662));
#14845=CARTESIAN_POINT('Ctrl Pts',(80.399431269224,0.883057219908353,329.147402087118));
#14846=CARTESIAN_POINT('Ctrl Pts',(80.3920222758392,0.726890339726405,329.128070079053));
#14847=CARTESIAN_POINT('Ctrl Pts',(80.384608718259,0.570627255359718,329.108726161804));
#14848=CARTESIAN_POINT('Ctrl Pts',(80.3771951606788,0.413731426320462,329.095641520972));
#14849=CARTESIAN_POINT('Ctrl Pts',(80.3697816030985,0.256741978943702,329.088822949805));
#14850=CARTESIAN_POINT('Ctrl Pts',(80.3623574909619,0.099529028347838,329.081994671155));
#14851=CARTESIAN_POINT('Ctrl Pts',(80.3549333788252,-0.0577774345755615,
329.081450280275));
#14852=CARTESIAN_POINT('Ctrl Pts',(80.3475092666885,-0.21464052778645,329.087144513323));
#14853=CARTESIAN_POINT('Ctrl Pts',(80.3436521415338,-0.296137220121997,
329.090102896644));
#14854=CARTESIAN_POINT('Ctrl Pts',(80.3397950163791,-0.377514346555329,
329.094744370205));
#14855=CARTESIAN_POINT('Ctrl Pts',(80.3359378912244,-0.458697606713513,
329.101057122832));
#14856=CARTESIAN_POINT('Ctrl Pts',(80.3285139137864,-0.614954577276633,
329.113207553836));
#14857=CARTESIAN_POINT('Ctrl Pts',(80.3210899363484,-0.770964157015842,
329.131589233217));
#14858=CARTESIAN_POINT('Ctrl Pts',(80.3136659589105,-0.926189318792645,
329.156190976062));
#14859=CARTESIAN_POINT('Ctrl Pts',(80.3062507428828,-1.08123129152422,329.18076368515));
#14860=CARTESIAN_POINT('Ctrl Pts',(80.2988355268552,-1.23549032395035,329.211541788247));
#14861=CARTESIAN_POINT('Ctrl Pts',(80.2914203108275,-1.38843192189614,329.248462174274));
#14862=CARTESIAN_POINT('Ctrl Pts',(80.2840122296834,-1.54122636020646,329.285347035691));
#14863=CARTESIAN_POINT('Ctrl Pts',(80.2766041485393,-1.69270552728362,329.32836232719));
#14864=CARTESIAN_POINT('Ctrl Pts',(80.2691960673952,-1.84234267767444,329.377393485178));
#14865=CARTESIAN_POINT('Ctrl Pts',(80.2617935002212,-1.99186845040183,329.426388148379));
#14866=CARTESIAN_POINT('Ctrl Pts',(80.2543909330472,-2.13955458325798,329.481389646566));
#14867=CARTESIAN_POINT('Ctrl Pts',(80.2469883658731,-2.28488721989842,329.5422329699));
#14868=CARTESIAN_POINT('Ctrl Pts',(80.2395896961184,-2.43014333954022,329.60304425949));
#14869=CARTESIAN_POINT('Ctrl Pts',(80.2321910263636,-2.57304808732545,329.669691105036));
#14870=CARTESIAN_POINT('Ctrl Pts',(80.2247923566089,-2.71310550645209,329.741959578573));
#14871=CARTESIAN_POINT('Ctrl Pts',(80.2173949074049,-2.85313982045348,329.814216130056));
#14872=CARTESIAN_POINT('Ctrl Pts',(80.2099974582009,-2.99032740670102,329.892092297984));
#14873=CARTESIAN_POINT('Ctrl Pts',(80.202600008997,-3.12419483295627,329.975327154109));
#14874=CARTESIAN_POINT('Ctrl Pts',(80.1952028805335,-3.25805645495331,330.058558401317));
#14875=CARTESIAN_POINT('Ctrl Pts',(80.18780575207,-3.38859788624905,330.147147677683));
#14876=CARTESIAN_POINT('Ctrl Pts',(80.1804086236066,-3.51537296808742,330.240789618252));
#14877=CARTESIAN_POINT('Ctrl Pts',(80.17301035617,-3.64216757012357,330.334445977342));
#14878=CARTESIAN_POINT('Ctrl Pts',(80.1656120887334,-3.76519436778241,330.43315632795));
#14879=CARTESIAN_POINT('Ctrl Pts',(80.1582138212968,-3.88403882521727,330.536573853338));
#14880=CARTESIAN_POINT('Ctrl Pts',(80.150812954771,-4.00292503396033,330.640027710391));
#14881=CARTESIAN_POINT('Ctrl Pts',(80.1434120882452,-4.11762569574288,330.748191789857));
#14882=CARTESIAN_POINT('Ctrl Pts',(80.1360112217195,-4.22776191320848,330.860681243523));
#14883=CARTESIAN_POINT('Ctrl Pts',(80.1286022283347,-4.33801907077005,330.973294221363));
#14884=CARTESIAN_POINT('Ctrl Pts',(80.12119323495,-4.44370151313924,331.090241791923));
#14885=CARTESIAN_POINT('Ctrl Pts',(80.1137842415652,-4.54446907087158,331.211104194308));
#14886=CARTESIAN_POINT('Ctrl Pts',(80.106370683985,-4.64529870489561,331.332041052102));
#14887=CARTESIAN_POINT('Ctrl Pts',(80.0989571264047,-4.74120719429455,331.456897252016));
#14888=CARTESIAN_POINT('Ctrl Pts',(80.0915435688244,-4.83189707428448,331.585223107431));
#14889=CARTESIAN_POINT('Ctrl Pts',(80.0841194566878,-4.9227160679212,331.713731658194));
#14890=CARTESIAN_POINT('Ctrl Pts',(80.0766953445511,-5.00830141115666,331.845719417711));
#14891=CARTESIAN_POINT('Ctrl Pts',(80.0692712324144,-5.08840062964462,331.980710415556));
#14892=CARTESIAN_POINT('Ctrl Pts',(80.0654141072598,-5.13001539849632,332.050843673763));
#14893=CARTESIAN_POINT('Ctrl Pts',(80.0615569821051,-5.17015011688825,332.121787203156));
#14894=CARTESIAN_POINT('Ctrl Pts',(80.0576998569504,-5.20877450889368,332.193472131263));
#14895=CARTESIAN_POINT('Ctrl Pts',(80.049875041618,-5.28713046641486,332.338896845801));
#14896=CARTESIAN_POINT('Ctrl Pts',(80.0420502262856,-5.35948338707886,332.487773869415));
#14897=CARTESIAN_POINT('Ctrl Pts',(80.0342254109531,-5.42553325429316,332.639593367858));
#14898=CARTESIAN_POINT('Ctrl Pts',(80.0264137334295,-5.49147222425392,332.791157962452));
#14899=CARTESIAN_POINT('Ctrl Pts',(80.0186020559058,-5.55112911112713,332.945654897665));
#14900=CARTESIAN_POINT('Ctrl Pts',(80.0107903783822,-5.60424943125671,333.102549374882));
#14901=CARTESIAN_POINT('Ctrl Pts',(80.0029966038673,-5.65724800883473,333.259084277197));
#14902=CARTESIAN_POINT('Ctrl Pts',(79.9952028293525,-5.70373979997366,333.418005465413));
#14903=CARTESIAN_POINT('Ctrl Pts',(79.9874090548376,-5.74351834540505,333.578758437669));
#14904=CARTESIAN_POINT('Ctrl Pts',(79.9796258163115,-5.78324311633875,333.739294096541));
#14905=CARTESIAN_POINT('Ctrl Pts',(79.9718425777854,-5.81627265272573,333.901656301376));
#14906=CARTESIAN_POINT('Ctrl Pts',(79.9640593392593,-5.84244959957532,334.065273709088));
#14907=CARTESIAN_POINT('Ctrl Pts',(79.9562906289864,-5.86857768433349,334.228585707282));
#14908=CARTESIAN_POINT('Ctrl Pts',(79.9485219187135,-5.88787864306747,334.393147926222));
#14909=CARTESIAN_POINT('Ctrl Pts',(79.9407532084407,-5.90024577640127,334.558377604102));
#14910=CARTESIAN_POINT('Ctrl Pts',(79.9338528072056,-5.91123063477968,334.705139554704));
#14911=CARTESIAN_POINT('Ctrl Pts',(79.9269524059706,-5.9167456887839,334.852427753432));
#14912=CARTESIAN_POINT('Ctrl Pts',(79.9200520047356,-5.91674999747214,334.99982704509));
#14913=CARTESIAN_POINT('',(78.1700520047036,-5.91674755306803,335.00538105598));
#14914=CARTESIAN_POINT('Ctrl Pts',(79.9200520047036,-5.91674999747216,334.999827045773));
#14915=CARTESIAN_POINT('Ctrl Pts',(79.9123202372434,-5.91675482525579,335.164985129787));
#14916=CARTESIAN_POINT('Ctrl Pts',(79.9045884697832,-5.90984009020886,335.3300164581));
#14917=CARTESIAN_POINT('Ctrl Pts',(79.8968567023231,-5.89606343540053,335.494334429544));
#14918=CARTESIAN_POINT('Ctrl Pts',(79.889115815794,-5.88227053200939,335.658846202328));
#14919=CARTESIAN_POINT('Ctrl Pts',(79.881374929265,-5.8615995840751,335.822642619378));
#14920=CARTESIAN_POINT('Ctrl Pts',(79.8736340427359,-5.83415972547376,335.985145095993));
#14921=CARTESIAN_POINT('Ctrl Pts',(79.865786357731,-5.80634128813123,336.149889566051));
#14922=CARTESIAN_POINT('Ctrl Pts',(79.857938672726,-5.77156587241067,336.313303792882));
#14923=CARTESIAN_POINT('Ctrl Pts',(79.8500909877211,-5.72999951188898,336.474800378442));
#14924=CARTESIAN_POINT('Ctrl Pts',(79.8423239099273,-5.68886009872801,336.634638157695));
#14925=CARTESIAN_POINT('Ctrl Pts',(79.8345568321335,-5.64106875826645,336.792597223523));
#14926=CARTESIAN_POINT('Ctrl Pts',(79.8267897543398,-5.58683534686467,336.948127657399));
#14927=CARTESIAN_POINT('Ctrl Pts',(79.8189017657292,-5.53175767894282,337.106079247892));
#14928=CARTESIAN_POINT('Ctrl Pts',(79.8110137771187,-5.47003586305808,337.261525649259));
#14929=CARTESIAN_POINT('Ctrl Pts',(79.8031257885081,-5.40193857534993,337.413915945232));
#14930=CARTESIAN_POINT('Ctrl Pts',(79.7952377998976,-5.33384128764181,337.566306241205));
#14931=CARTESIAN_POINT('Ctrl Pts',(79.787349811287,-5.25936873664166,337.715640155412));
#14932=CARTESIAN_POINT('Ctrl Pts',(79.7794618226765,-5.17883592564806,337.861396340551));
#14933=CARTESIAN_POINT('Ctrl Pts',(79.7720378452385,-5.10304045973776,337.998578413616));
#14934=CARTESIAN_POINT('Ctrl Pts',(79.7646138678006,-5.02167616900644,338.13295373613));
#14935=CARTESIAN_POINT('Ctrl Pts',(79.7571898903626,-4.93497572224292,338.264038171249));
#14936=CARTESIAN_POINT('Ctrl Pts',(79.749774674335,-4.84837759505124,338.394967907013));
#14937=CARTESIAN_POINT('Ctrl Pts',(79.7423594583074,-4.75645605091942,338.522614177775));
#14938=CARTESIAN_POINT('Ctrl Pts',(79.7349442422799,-4.65948996940092,338.646516664922));
#14939=CARTESIAN_POINT('Ctrl Pts',(79.7275361611358,-4.56261718815782,338.77029993372));
#14940=CARTESIAN_POINT('Ctrl Pts',(79.7201280799917,-4.46070976107004,338.890346298368));
#14941=CARTESIAN_POINT('Ctrl Pts',(79.7127199988477,-4.35409018648798,339.006223809328));
#14942=CARTESIAN_POINT('Ctrl Pts',(79.7053174316737,-4.24754997080285,339.122015070541));
#14943=CARTESIAN_POINT('Ctrl Pts',(79.6979148644997,-4.13630484286159,339.233643383032));
#14944=CARTESIAN_POINT('Ctrl Pts',(79.6905122973258,-4.02071787431496,339.340709427924));
#14945=CARTESIAN_POINT('Ctrl Pts',(79.683113627571,-3.90519176180136,339.447719103012));
#14946=CARTESIAN_POINT('Ctrl Pts',(79.6757149578163,-3.78532863441719,339.550171041278));
#14947=CARTESIAN_POINT('Ctrl Pts',(79.6683162880615,-3.66152867050092,339.647702481614));
#14948=CARTESIAN_POINT('Ctrl Pts',(79.6609188388576,-3.53774912973494,339.745217832291));
#14949=CARTESIAN_POINT('Ctrl Pts',(79.6535213896537,-3.41003433427522,339.837814065324));
#14950=CARTESIAN_POINT('Ctrl Pts',(79.6461239404497,-3.27881790750221,339.925168392242));
#14951=CARTESIAN_POINT('Ctrl Pts',(79.6387268119863,-3.14760717004481,340.012518931629));
#14952=CARTESIAN_POINT('Ctrl Pts',(79.6313296835228,-3.01289541381673,340.094627809989));
#14953=CARTESIAN_POINT('Ctrl Pts',(79.6239325550594,-2.87514540656207,340.171215471591));
#14954=CARTESIAN_POINT('Ctrl Pts',(79.6165342876228,-2.7373741892447,340.247814925782));
#14955=CARTESIAN_POINT('Ctrl Pts',(79.6091360201863,-2.59656411562483,340.318891289129));
#14956=CARTESIAN_POINT('Ctrl Pts',(79.6017377527497,-2.45320257915038,340.384210960591));
#14957=CARTESIAN_POINT('Ctrl Pts',(79.5943368862239,-2.30979067826044,340.449553579541));
#14958=CARTESIAN_POINT('Ctrl Pts',(79.5869360196982,-2.1638258692795,340.509135325395));
#14959=CARTESIAN_POINT('Ctrl Pts',(79.5795351531724,-2.01581539474792,340.562770789525));
#14960=CARTESIAN_POINT('Ctrl Pts',(79.5721261597877,-1.86764239056515,340.616465150523));
#14961=CARTESIAN_POINT('Ctrl Pts',(79.564717166403,-1.71741958587069,340.664200062636));
#14962=CARTESIAN_POINT('Ctrl Pts',(79.5573081730183,-1.56566995381436,340.705839829352));
#14963=CARTESIAN_POINT('Ctrl Pts',(79.549894615438,-1.41382683875039,340.747505247601));
#14964=CARTESIAN_POINT('Ctrl Pts',(79.5424810578578,-1.26045538481414,340.783067954373));
#14965=CARTESIAN_POINT('Ctrl Pts',(79.5350675002776,-1.10608810937295,340.81244351859));
#14966=CARTESIAN_POINT('Ctrl Pts',(79.527643388141,-0.951501063854682,340.841860904302));
#14967=CARTESIAN_POINT('Ctrl Pts',(79.5202192760043,-0.795915733462748,
340.865073500139));
#14968=CARTESIAN_POINT('Ctrl Pts',(79.5127951638677,-0.639869918127623,
340.882048712003));
#14969=CARTESIAN_POINT('Ctrl Pts',(79.5089380387126,-0.55879783454485,340.890868018001));
#14970=CARTESIAN_POINT('Ctrl Pts',(79.5050809135576,-0.477601470499032,
340.898004575316));
#14971=CARTESIAN_POINT('Ctrl Pts',(79.5012237884025,-0.396356052928012,
340.903459362256));
#14972=CARTESIAN_POINT('Ctrl Pts',(79.4937998109645,-0.239979445288353,
340.913958429188));
#14973=CARTESIAN_POINT('Ctrl Pts',(79.4863758335265,-0.0829494834163334,
340.918255658748));
#14974=CARTESIAN_POINT('Ctrl Pts',(79.4789518560885,0.0742008012545575,
340.916284712858));
#14975=CARTESIAN_POINT('Ctrl Pts',(79.4715366400609,0.23116562494422,340.91431609298));
#14976=CARTESIAN_POINT('Ctrl Pts',(79.4641214240333,0.388250119228613,340.90609402691));
#14977=CARTESIAN_POINT('Ctrl Pts',(79.4567062080057,0.544916274636628,340.891603925599));
#14978=CARTESIAN_POINT('Ctrl Pts',(79.4492981268616,0.701431686659512,340.877127766591));
#14979=CARTESIAN_POINT('Ctrl Pts',(79.4418900457175,0.857529192013971,340.856395613223));
#14980=CARTESIAN_POINT('Ctrl Pts',(79.4344819645734,1.01267103275587,340.829444908558));
#14981=CARTESIAN_POINT('Ctrl Pts',(79.4270793973994,1.16769739859159,340.802514263796));
#14982=CARTESIAN_POINT('Ctrl Pts',(79.4196768302254,1.3217691500244,340.769374347519));
#14983=CARTESIAN_POINT('Ctrl Pts',(79.4122742630514,1.47435401238794,340.730114380067));
#14984=CARTESIAN_POINT('Ctrl Pts',(79.4048755932967,1.62685853948896,340.690875082817));
#14985=CARTESIAN_POINT('Ctrl Pts',(79.3974769235419,1.77787737606564,340.645522244318));
#14986=CARTESIAN_POINT('Ctrl Pts',(79.3900782537872,1.92688890910211,340.594196072223));
#14987=CARTESIAN_POINT('Ctrl Pts',(79.3826808045832,2.0758758598628,340.542878367353));
#14988=CARTESIAN_POINT('Ctrl Pts',(79.3752833553792,2.22285581177223,340.48558940604));
#14989=CARTESIAN_POINT('Ctrl Pts',(79.3678859061752,2.36732266662489,340.422519152072));
#14990=CARTESIAN_POINT('Ctrl Pts',(79.3604887777118,2.51178325764637,340.35945163272));
#14991=CARTESIAN_POINT('Ctrl Pts',(79.3530916492483,2.65373062622977,340.290603468445));
#14992=CARTESIAN_POINT('Ctrl Pts',(79.3456945207848,2.79267925781721,340.216212526868));
#14993=CARTESIAN_POINT('Ctrl Pts',(79.3382962533482,2.93164928402549,340.141810130944));
#14994=CARTESIAN_POINT('Ctrl Pts',(79.3308979859116,3.06761932482788,340.061863434553));
#14995=CARTESIAN_POINT('Ctrl Pts',(79.3234997184749,3.20012918356456,339.976655882317));
#14996=CARTESIAN_POINT('Ctrl Pts',(79.3160988519492,3.33268559440775,339.891418395772));
#14997=CARTESIAN_POINT('Ctrl Pts',(79.3086979854235,3.46177908921587,339.800916575358));
#14998=CARTESIAN_POINT('Ctrl Pts',(79.3012971188977,3.58697925587329,339.705476636902));
#14999=CARTESIAN_POINT('Ctrl Pts',(79.293888125513,3.71231690428348,339.609931896269));
#15000=CARTESIAN_POINT('Ctrl Pts',(79.2864791321282,3.83375238966257,339.509438434912));
#15001=CARTESIAN_POINT('Ctrl Pts',(79.2790701387435,3.95088859113733,339.404362598938));
#15002=CARTESIAN_POINT('Ctrl Pts',(79.2716565811632,4.06809695255291,339.299222032624));
#15003=CARTESIAN_POINT('Ctrl Pts',(79.264243023583,4.18100048555196,339.189493726194));
#15004=CARTESIAN_POINT('Ctrl Pts',(79.2568294660027,4.28924001453668,339.07557979436));
#15005=CARTESIAN_POINT('Ctrl Pts',(79.249405353866,4.39763364230674,338.96150368519));
#15006=CARTESIAN_POINT('Ctrl Pts',(79.2419812417293,4.50134975912482,338.843230329141));
#15007=CARTESIAN_POINT('Ctrl Pts',(79.2345571295926,4.60006992151687,338.72119433511));
#15008=CARTESIAN_POINT('Ctrl Pts',(79.230700004438,4.6513590204187,338.657791722961));
#15009=CARTESIAN_POINT('Ctrl Pts',(79.2268428792833,4.70130031534411,338.593373968852));
#15010=CARTESIAN_POINT('Ctrl Pts',(79.2229857541286,4.74985391935847,338.528004862136));
#15011=CARTESIAN_POINT('Ctrl Pts',(79.2155617766906,4.84330716401107,338.402186084176));
#15012=CARTESIAN_POINT('Ctrl Pts',(79.2081377992526,4.93189871877175,338.27246171664));
#15013=CARTESIAN_POINT('Ctrl Pts',(79.2007138218146,5.01528434464131,338.139244097692));
#15014=CARTESIAN_POINT('Ctrl Pts',(79.1932986057869,5.09857156292619,338.006183695578));
#15015=CARTESIAN_POINT('Ctrl Pts',(79.1858833897593,5.17666488552189,337.869638561351));
#15016=CARTESIAN_POINT('Ctrl Pts',(79.1784681737317,5.2492608963903,337.73005322368));
#15017=CARTESIAN_POINT('Ctrl Pts',(79.1710600925876,5.32178705574251,337.590602194319));
#15018=CARTESIAN_POINT('Ctrl Pts',(79.1636520114435,5.38882626269449,337.448117114075));
#15019=CARTESIAN_POINT('Ctrl Pts',(79.1562439302994,5.45011899223641,337.303070457664));
#15020=CARTESIAN_POINT('Ctrl Pts',(79.1488413631254,5.51136610048038,337.158131762128));
#15021=CARTESIAN_POINT('Ctrl Pts',(79.1414387959514,5.56687510320979,337.010635629106));
#15022=CARTESIAN_POINT('Ctrl Pts',(79.1340362287774,5.61643298334764,336.861077941964));
#15023=CARTESIAN_POINT('Ctrl Pts',(79.1266375590227,5.66596477147812,336.711598996291));
#15024=CARTESIAN_POINT('Ctrl Pts',(79.1192388892679,5.70955155995479,336.560061011511));
#15025=CARTESIAN_POINT('Ctrl Pts',(79.1118402195132,5.74702897765007,336.406978497544));
#15026=CARTESIAN_POINT('Ctrl Pts',(79.1044427703092,5.78450021273525,336.253921237437));
#15027=CARTESIAN_POINT('Ctrl Pts',(79.0970453211052,5.81586398864669,336.09932031599));
#15028=CARTESIAN_POINT('Ctrl Pts',(79.0896478719012,5.84100617120702,335.943704122287));
#15029=CARTESIAN_POINT('Ctrl Pts',(79.0822507434378,5.86614726364613,335.788094675831));
#15030=CARTESIAN_POINT('Ctrl Pts',(79.0748536149743,5.8850672395747,335.631470413078));
#15031=CARTESIAN_POINT('Ctrl Pts',(79.0674564865108,5.89770338716464,335.474368337399));
#15032=CARTESIAN_POINT('Ctrl Pts',(79.0600582190742,5.91034148040587,335.317242071922));
#15033=CARTESIAN_POINT('Ctrl Pts',(79.0526599516376,5.9166937888601,335.15963821906));
#15034=CARTESIAN_POINT('Ctrl Pts',(79.045261684201,5.91674962833785,335.002097156152));
#15035=CARTESIAN_POINT('Ctrl Pts',(79.0378608176752,5.9168054874326,334.84450074741));
#15036=CARTESIAN_POINT('Ctrl Pts',(79.0304599511494,5.91056047329898,334.686967545517));
#15037=CARTESIAN_POINT('Ctrl Pts',(79.0230590846236,5.89805598709171,334.530036027305));
#15038=CARTESIAN_POINT('Ctrl Pts',(79.0156500912388,5.88553776976313,334.372932183282));
#15039=CARTESIAN_POINT('Ctrl Pts',(79.0082410978541,5.86674638327842,334.21643171466));
#15040=CARTESIAN_POINT('Ctrl Pts',(79.0008321044693,5.84177499100484,334.061066819752));
#15041=CARTESIAN_POINT('Ctrl Pts',(78.993418546889,5.81678821549222,333.90560621471));
#15042=CARTESIAN_POINT('Ctrl Pts',(78.9860049893088,5.78561392177289,333.751282942301));
#15043=CARTESIAN_POINT('Ctrl Pts',(78.9785914317285,5.74839588616332,333.598616648293));
#15044=CARTESIAN_POINT('Ctrl Pts',(78.9711673195918,5.71112486386649,333.445733005867));
#15045=CARTESIAN_POINT('Ctrl Pts',(78.9637432074551,5.66779301755273,333.294511411067));
#15046=CARTESIAN_POINT('Ctrl Pts',(78.9563190953184,5.61859349108032,333.145454841615));
#15047=CARTESIAN_POINT('Ctrl Pts',(78.9524619701639,5.59303235627328,333.068013952671));
#15048=CARTESIAN_POINT('Ctrl Pts',(78.9486048450093,5.56588819286609,332.991157109282));
#15049=CARTESIAN_POINT('Ctrl Pts',(78.9447477198548,5.53719305757851,332.914952373301));
#15050=CARTESIAN_POINT('Ctrl Pts',(78.9373237424168,5.48196227599398,332.768277785901));
#15051=CARTESIAN_POINT('Ctrl Pts',(78.9298997649788,5.42081626144866,332.623577958629));
#15052=CARTESIAN_POINT('Ctrl Pts',(78.9224757875408,5.35391547042627,332.481365509243));
#15053=CARTESIAN_POINT('Ctrl Pts',(78.9150605715132,5.2870936324032,332.339320891945));
#15054=CARTESIAN_POINT('Ctrl Pts',(78.9076453554855,5.21453069381927,332.199758143838));
#15055=CARTESIAN_POINT('Ctrl Pts',(78.9002301394579,5.13643627248911,332.063172973912));
#15056=CARTESIAN_POINT('Ctrl Pts',(78.8928220583138,5.05841699321783,331.92671922555));
#15057=CARTESIAN_POINT('Ctrl Pts',(78.8854139771697,4.97487701104492,331.793237673493));
#15058=CARTESIAN_POINT('Ctrl Pts',(78.8780058960257,4.8860731961658,331.663202241039));
#15059=CARTESIAN_POINT('Ctrl Pts',(78.8706033288516,4.79733547958791,331.533263596332));
#15060=CARTESIAN_POINT('Ctrl Pts',(78.8632007616777,4.70334194112026,331.406766270799));
#15061=CARTESIAN_POINT('Ctrl Pts',(78.8557981945036,4.60439430390263,331.28415774599));
#15062=CARTESIAN_POINT('Ctrl Pts',(78.8483995247489,4.50549876218306,331.161613774032));
#15063=CARTESIAN_POINT('Ctrl Pts',(78.8410008549941,4.40165455011443,331.042954814906));
#15064=CARTESIAN_POINT('Ctrl Pts',(78.8336021852393,4.29320537941507,330.928597522639));
#15065=CARTESIAN_POINT('Ctrl Pts',(78.8262047360354,4.18477409946197,330.814259095775));
#15066=CARTESIAN_POINT('Ctrl Pts',(78.8188072868314,4.07173962515045,330.704221197901));
#15067=CARTESIAN_POINT('Ctrl Pts',(78.8114098376274,3.95448452558128,330.598865748533));
#15068=CARTESIAN_POINT('Ctrl Pts',(78.8040127091639,3.83723450998864,330.493514867193));
#15069=CARTESIAN_POINT('Ctrl Pts',(78.7966155807005,3.71576451061122,330.392846280121));
#15070=CARTESIAN_POINT('Ctrl Pts',(78.789218452237,3.59049216806972,330.297203326367));
#15071=CARTESIAN_POINT('Ctrl Pts',(78.7818201848004,3.46520053671504,330.201545645986));
#15072=CARTESIAN_POINT('Ctrl Pts',(78.7744219173638,3.33610569311327,330.110915366196));
#15073=CARTESIAN_POINT('Ctrl Pts',(78.7670236499272,3.20365627026824,330.025613900744));
#15074=CARTESIAN_POINT('Ctrl Pts',(78.7596227834015,3.07116031654838,329.94028246799));
#15075=CARTESIAN_POINT('Ctrl Pts',(78.7522219168758,2.9353077507679,329.86028377881));
#15076=CARTESIAN_POINT('Ctrl Pts',(78.7448210503501,2.79657379412326,329.7858744188));
#15077=CARTESIAN_POINT('Ctrl Pts',(78.7374120569653,2.65768749433004,329.711383350199));
#15078=CARTESIAN_POINT('Ctrl Pts',(78.7300030635806,2.51591381399847,329.642494044424));
#15079=CARTESIAN_POINT('Ctrl Pts',(78.7225940701958,2.37175070608923,329.579416161458));
#15080=CARTESIAN_POINT('Ctrl Pts',(78.7151805126156,2.22749878873341,329.51629942034));
#15081=CARTESIAN_POINT('Ctrl Pts',(78.7077669550354,2.08085485751147,329.459001371235));
#15082=CARTESIAN_POINT('Ctrl Pts',(78.7003533974552,1.93233369925061,329.407682319714));
#15083=CARTESIAN_POINT('Ctrl Pts',(78.6929292853185,1.7836010939302,329.356290206127));
#15084=CARTESIAN_POINT('Ctrl Pts',(78.6855051731819,1.63298628027064,329.310894198097));
#15085=CARTESIAN_POINT('Ctrl Pts',(78.6780810610452,1.48101674419461,329.271604066939));
#15086=CARTESIAN_POINT('Ctrl Pts',(78.6742239358904,1.4020624518061,329.251191261954));
#15087=CARTESIAN_POINT('Ctrl Pts',(78.6703668107356,1.32274262817448,329.232425720055));
#15088=CARTESIAN_POINT('Ctrl Pts',(78.6665096855808,1.24313185569531,329.215317316235));
#15089=CARTESIAN_POINT('Ctrl Pts',(78.6590857081428,1.08990152092884,329.182388023338));
#15090=CARTESIAN_POINT('Ctrl Pts',(78.6516617307048,0.935130732112104,329.155501632051));
#15091=CARTESIAN_POINT('Ctrl Pts',(78.6442377532668,0.779337392664969,329.134800617976));
#15092=CARTESIAN_POINT('Ctrl Pts',(78.6368225372391,0.623727912798643,329.114124034212));
#15093=CARTESIAN_POINT('Ctrl Pts',(78.6294073212115,0.467098650745942,329.09961834622));
#15094=CARTESIAN_POINT('Ctrl Pts',(78.6219921051838,0.309979894999703,329.091375538486));
#15095=CARTESIAN_POINT('Ctrl Pts',(78.6145840240398,0.153012318129479,329.083140661941));
#15096=CARTESIAN_POINT('Ctrl Pts',(78.6071759428957,-0.00444344457639809,
329.081156688209));
#15097=CARTESIAN_POINT('Ctrl Pts',(78.5997678617516,-0.16184985370418,329.085464076755));
#15098=CARTESIAN_POINT('Ctrl Pts',(78.5923652945775,-0.31913910236706,329.089768259233));
#15099=CARTESIAN_POINT('Ctrl Pts',(78.5849627274035,-0.47637869912249,329.100354469734));
#15100=CARTESIAN_POINT('Ctrl Pts',(78.5775601602295,-0.633029067485845,
329.117211140775));
#15101=CARTESIAN_POINT('Ctrl Pts',(78.5701614904748,-0.78959696011467,329.134058936853));
#15102=CARTESIAN_POINT('Ctrl Pts',(78.5627628207201,-0.9455758720507,329.157170578768));
#15103=CARTESIAN_POINT('Ctrl Pts',(78.5553641509653,-1.10042942790038,329.186482507405));
#15104=CARTESIAN_POINT('Ctrl Pts',(78.5479667017613,-1.25525743772258,329.215789600484));
#15105=CARTESIAN_POINT('Ctrl Pts',(78.5405692525574,-1.40896009356819,329.251294880904));
#15106=CARTESIAN_POINT('Ctrl Pts',(78.5331718033534,-1.56100920107542,329.292883316713));
#15107=CARTESIAN_POINT('Ctrl Pts',(78.5257746748899,-1.71305171599789,329.334469949319));
#15108=CARTESIAN_POINT('Ctrl Pts',(78.5183775464264,-1.86344046514696,329.382139114417));
#15109=CARTESIAN_POINT('Ctrl Pts',(78.5109804179629,-2.0116607180864,329.435725409561));
#15110=CARTESIAN_POINT('Ctrl Pts',(78.5035821505263,-2.15990379324502,329.489319955656));
#15111=CARTESIAN_POINT('Ctrl Pts',(78.4961838830897,-2.30597735636702,329.548833319));
#15112=CARTESIAN_POINT('Ctrl Pts',(78.4887856156531,-2.44938516114103,329.614051346802));
#15113=CARTESIAN_POINT('Ctrl Pts',(78.4813847491273,-2.59284334658487,329.679292286383));
#15114=CARTESIAN_POINT('Ctrl Pts',(78.4739838826015,-2.73363356957718,329.750241726197));
#15115=CARTESIAN_POINT('Ctrl Pts',(78.4665830160758,-2.87128289235744,329.82663889579));
#15116=CARTESIAN_POINT('Ctrl Pts',(78.459174022691,-3.0090833672544,329.903119956779));
#15117=CARTESIAN_POINT('Ctrl Pts',(78.4517650293062,-3.14373572756957,329.985060512957));
#15118=CARTESIAN_POINT('Ctrl Pts',(78.4443560359214,-3.27479419483106,330.072155284102));
#15119=CARTESIAN_POINT('Ctrl Pts',(78.4369424783412,-3.4059333986289,330.159303708631));
#15120=CARTESIAN_POINT('Ctrl Pts',(78.4295289207609,-3.53347399613346,330.251612456776));
#15121=CARTESIAN_POINT('Ctrl Pts',(78.4221153631806,-3.65700260227987,330.348735383853));
#15122=CARTESIAN_POINT('Ctrl Pts',(78.4146912510439,-3.78070707401207,330.445996583199));
#15123=CARTESIAN_POINT('Ctrl Pts',(78.4072671389072,-3.90038786359415,330.548085408464));
#15124=CARTESIAN_POINT('Ctrl Pts',(78.3998430267705,-4.0156672090846,330.654617689042));
#15125=CARTESIAN_POINT('Ctrl Pts',(78.3959859016159,-4.07555947028801,330.709965497862));
#15126=CARTESIAN_POINT('Ctrl Pts',(78.3921287764613,-4.13426432275085,330.766512118276));
#15127=CARTESIAN_POINT('Ctrl Pts',(78.3882716513067,-4.19173310156535,330.824200176285));
#15128=CARTESIAN_POINT('Ctrl Pts',(78.3809497166853,-4.30082539813059,330.933708727926));
#15129=CARTESIAN_POINT('Ctrl Pts',(78.3736277820639,-4.40581013785178,331.04768289274));
#15130=CARTESIAN_POINT('Ctrl Pts',(78.3663058474424,-4.50629201713378,331.165777416631));
#15131=CARTESIAN_POINT('Ctrl Pts',(78.3589927243679,-4.60665297198342,331.283729820238));
#15132=CARTESIAN_POINT('Ctrl Pts',(78.3516796012933,-4.7025216017473,331.405792427091));
#15133=CARTESIAN_POINT('Ctrl Pts',(78.3443664782187,-4.79353790424402,331.531581783712));
#15134=CARTESIAN_POINT('Ctrl Pts',(78.3370616527893,-4.88445093745738,331.657228416708));
#15135=CARTESIAN_POINT('Ctrl Pts',(78.3297568273599,-4.97052238337176,331.78659306962));
#15136=CARTESIAN_POINT('Ctrl Pts',(78.3224520019304,-5.05143148884183,331.919258128951));
#15137=CARTESIAN_POINT('Ctrl Pts',(78.3151518665795,-5.13228864645006,332.0518380104));
#15138=CARTESIAN_POINT('Ctrl Pts',(78.3078517312287,-5.20798985723673,332.187713756579));
#15139=CARTESIAN_POINT('Ctrl Pts',(78.3005515958778,-5.27825672391012,332.326437485489));
#15140=CARTESIAN_POINT('Ctrl Pts',(78.2932546132463,-5.3484932443361,332.465101303593));
#15141=CARTESIAN_POINT('Ctrl Pts',(78.2859576306148,-5.41329991681757,332.606610315089));
#15142=CARTESIAN_POINT('Ctrl Pts',(78.2786606479834,-5.47244364816107,332.750490924623));
#15143=CARTESIAN_POINT('Ctrl Pts',(78.2713652833192,-5.53157426550559,332.894339631366));
#15144=CARTESIAN_POINT('Ctrl Pts',(78.264069918655,-5.58504429525359,333.040558534064));
#15145=CARTESIAN_POINT('Ctrl Pts',(78.2567745539908,-5.63266839287065,333.188653170026));
#15146=CARTESIAN_POINT('Ctrl Pts',(78.2494767028018,-5.68030872250736,333.336798282012));
#15147=CARTESIAN_POINT('Ctrl Pts',(78.2421788516127,-5.72209901513291,333.486820040269));
#15148=CARTESIAN_POINT('Ctrl Pts',(78.2348810004237,-5.75790345231781,333.638207653022));
#15149=CARTESIAN_POINT('Ctrl Pts',(78.2275821132039,-5.79371297243669,333.789616757337));
#15150=CARTESIAN_POINT('Ctrl Pts',(78.2202832259842,-5.82353486460667,333.942391726058));
#15151=CARTESIAN_POINT('Ctrl Pts',(78.2129843387645,-5.84728441350013,334.096011310835));
#15152=CARTESIAN_POINT('Ctrl Pts',(78.2056786537645,-5.87105608141101,334.249773968404));
#15153=CARTESIAN_POINT('Ctrl Pts',(78.1983729687645,-5.88874405596246,334.404382432076));
#15154=CARTESIAN_POINT('Ctrl Pts',(78.1910672837646,-5.90031545013051,334.559309460674));
#15155=CARTESIAN_POINT('Ctrl Pts',(78.1840621907443,-5.9114107399661,334.707862025793));
#15156=CARTESIAN_POINT('Ctrl Pts',(78.177057097724,-5.91688276630358,334.856707155613));
#15157=CARTESIAN_POINT('Ctrl Pts',(78.1700520047036,-5.91674755306803,335.00538105598));
#15158=CARTESIAN_POINT('',(76.4200520047036,-5.92511437741598,334.99740540478));
#15159=CARTESIAN_POINT('Ctrl Pts',(78.1700520047036,-5.91776632301522,335.005381982512));
#15160=CARTESIAN_POINT('Ctrl Pts',(78.15004587548,-5.92170700115339,335.430062848705));
#15161=CARTESIAN_POINT('Ctrl Pts',(78.0372937348318,-5.68602897212947,337.819173824506));
#15162=CARTESIAN_POINT('Ctrl Pts',(77.831795582759,-2.44063524270045,341.557127613012));
#15163=CARTESIAN_POINT('Ctrl Pts',(77.5535575484851,4.19326072651748,340.600820243559));
#15164=CARTESIAN_POINT('Ctrl Pts',(77.275319514211,6.97906321943746,334.504722804564));
#15165=CARTESIAN_POINT('Ctrl Pts',(76.997081479937,3.36028240668291,328.863133937542));
#15166=CARTESIAN_POINT('Ctrl Pts',(76.7188434456631,-3.34217997299833,328.853256476042));
#15167=CARTESIAN_POINT('Ctrl Pts',(76.5265002872521,-5.85529074220202,332.745839943748));
#15168=CARTESIAN_POINT('Ctrl Pts',(76.4269031402655,-5.92590944952505,334.852441329886));
#15169=CARTESIAN_POINT('Ctrl Pts',(76.4200520047036,-5.92511437741598,334.99740540478));
#15170=CARTESIAN_POINT('',(74.6700520047036,-5.9098640687304,334.996010226465));
#15171=CARTESIAN_POINT('Ctrl Pts',(76.4200520047036,-5.92511437741598,334.99740540478));
#15172=CARTESIAN_POINT('Ctrl Pts',(76.3341571288408,-5.91514630431429,336.81486633591));
#15173=CARTESIAN_POINT('Ctrl Pts',(76.1555162415536,-4.04647218064248,340.612465457021));
#15174=CARTESIAN_POINT('Ctrl Pts',(75.8841293428413,2.42129812204568,341.564292675178));
#15175=CARTESIAN_POINT('Ctrl Pts',(75.6058913085675,6.83035710149624,336.516194178614));
#15176=CARTESIAN_POINT('Ctrl Pts',(75.3276532742934,4.97129818480821,330.076706663327));
#15177=CARTESIAN_POINT('Ctrl Pts',(75.0494152400195,-1.44984769983852,328.155252775411));
#15178=CARTESIAN_POINT('Ctrl Pts',(74.8302148168229,-5.4603378352444,331.590028565428));
#15179=CARTESIAN_POINT('Ctrl Pts',(74.7037604050509,-5.91430140141107,334.278035342772));
#15180=CARTESIAN_POINT('Ctrl Pts',(74.6700520047036,-5.9098640687304,334.996010226465));
#15181=CARTESIAN_POINT('',(72.9200519871268,-5.91377486651518,335.004343153495));
#15182=CARTESIAN_POINT('Ctrl Pts',(74.6700520047036,-5.9098640687304,334.996010226465));
#15183=CARTESIAN_POINT('Ctrl Pts',(74.6110143936263,-5.90209242966351,336.253486745966));
#15184=CARTESIAN_POINT('Ctrl Pts',(74.4592307711244,-4.89277859890401,339.497807759121));
#15185=CARTESIAN_POINT('Ctrl Pts',(74.2147011371977,0.448117352137371,341.982249906723));
#15186=CARTESIAN_POINT('Ctrl Pts',(73.9364631029237,6.11402491854263,338.401664624365));
#15187=CARTESIAN_POINT('Ctrl Pts',(73.6582250686499,6.16918206006022,331.699421924716));
#15188=CARTESIAN_POINT('Ctrl Pts',(73.3799870343759,0.562971882037213,328.026071008301));
#15189=CARTESIAN_POINT('Ctrl Pts',(73.1339293463939,-4.8517161019475,330.437248912705));
#15190=CARTESIAN_POINT('Ctrl Pts',(72.9806176698364,-5.90182657715511,333.714701501588));
#15191=CARTESIAN_POINT('Ctrl Pts',(72.9200520047036,-5.91056552183396,335.004340422057));
#15192=CARTESIAN_POINT('',(71.1700520047036,-5.9210755085991,335.002052628764));
#15193=CARTESIAN_POINT('Ctrl Pts',(72.9200519708414,-5.91674840410918,335.00434568424));
#15194=CARTESIAN_POINT('Ctrl Pts',(72.9115360439865,-5.91661508257688,335.185865997231));
#15195=CARTESIAN_POINT('Ctrl Pts',(72.9030201171316,-5.90812453106049,335.367048315781));
#15196=CARTESIAN_POINT('Ctrl Pts',(72.8945041902767,-5.89139359093756,335.547185635009));
#15197=CARTESIAN_POINT('Ctrl Pts',(72.8859464929619,-5.87458058587037,335.728206524374));
#15198=CARTESIAN_POINT('Ctrl Pts',(72.8773887956471,-5.84944626172956,335.908172011056));
#15199=CARTESIAN_POINT('Ctrl Pts',(72.8688310983323,-5.81615864682976,336.086383522246));
#15200=CARTESIAN_POINT('Ctrl Pts',(72.8602189075065,-5.78265906381012,336.265729844659));
#15201=CARTESIAN_POINT('Ctrl Pts',(72.8516067166807,-5.74090210412475,336.443299656695));
#15202=CARTESIAN_POINT('Ctrl Pts',(72.8429945258548,-5.69110759812134,336.618401949179));
#15203=CARTESIAN_POINT('Ctrl Pts',(72.8365000058459,-5.65355717429603,336.750447948291));
#15204=CARTESIAN_POINT('Ctrl Pts',(72.8300054858369,-5.61143697585951,336.881091143479));
#15205=CARTESIAN_POINT('Ctrl Pts',(72.823510965828,-5.56485894612647,337.010043649331));
#15206=CARTESIAN_POINT('Ctrl Pts',(72.81608698839,-5.51161494328004,337.157451077854));
#15207=CARTESIAN_POINT('Ctrl Pts',(72.8086630109521,-5.4524295661987,337.302963847902));
#15208=CARTESIAN_POINT('Ctrl Pts',(72.8012390335141,-5.38745633068201,337.446067220559));
#15209=CARTESIAN_POINT('Ctrl Pts',(72.7938238174865,-5.32255977335893,337.589001709706));
#15210=CARTESIAN_POINT('Ctrl Pts',(72.7864086014589,-5.25188910669696,337.729532124879));
#15211=CARTESIAN_POINT('Ctrl Pts',(72.7789933854313,-5.17564723179545,337.867159970164));
#15212=CARTESIAN_POINT('Ctrl Pts',(72.7715853042873,-5.09947871644215,338.004655390629));
#15213=CARTESIAN_POINT('Ctrl Pts',(72.7641772231432,-5.0177498444251,338.139253476944));
#15214=CARTESIAN_POINT('Ctrl Pts',(72.7567691419992,-4.93071105926034,338.270476878467));
#15215=CARTESIAN_POINT('Ctrl Pts',(72.7493665748252,-4.84373705865302,338.401602608016));
#15216=CARTESIAN_POINT('Ctrl Pts',(72.7419640076512,-4.75146121984235,338.52935834453));
#15217=CARTESIAN_POINT('Ctrl Pts',(72.7345614404773,-4.6541791924521,338.653292570688));
#15218=CARTESIAN_POINT('Ctrl Pts',(72.7271627707225,-4.55694838362404,338.777161546018));
#15219=CARTESIAN_POINT('Ctrl Pts',(72.7197641009678,-4.45471686530048,338.897212725196));
#15220=CARTESIAN_POINT('Ctrl Pts',(72.7123654312131,-4.34782268836525,339.013024848295));
#15221=CARTESIAN_POINT('Ctrl Pts',(72.7049679820092,-4.24094614565005,339.128817865991));
#15222=CARTESIAN_POINT('Ctrl Pts',(72.6975705328052,-4.1294087238083,339.240372941537));
#15223=CARTESIAN_POINT('Ctrl Pts',(72.6901730836013,-4.01358779686133,339.347303021344));
#15224=CARTESIAN_POINT('Ctrl Pts',(72.6827759551379,-3.89777189170792,339.454228464849));
#15225=CARTESIAN_POINT('Ctrl Pts',(72.6753788266745,-3.77767312494759,339.556529058171));
#15226=CARTESIAN_POINT('Ctrl Pts',(72.667981698211,-3.65370446018548,339.65385585081));
#15227=CARTESIAN_POINT('Ctrl Pts',(72.6605834307745,-3.5297167073434,339.751197629346));
#15228=CARTESIAN_POINT('Ctrl Pts',(72.6531851633379,-3.40185816361799,339.843563851829));
#15229=CARTESIAN_POINT('Ctrl Pts',(72.6457868959013,-3.27057334862619,339.930647070492));
#15230=CARTESIAN_POINT('Ctrl Pts',(72.6383860293756,-3.13924241189826,340.017760882406));
#15231=CARTESIAN_POINT('Ctrl Pts',(72.6309851628499,-3.00448311818376,340.09958778909));
#15232=CARTESIAN_POINT('Ctrl Pts',(72.6235842963241,-2.86676717854363,340.175864807597));
#15233=CARTESIAN_POINT('Ctrl Pts',(72.6161753029394,-2.7289000136356,340.252225585564));
#15234=CARTESIAN_POINT('Ctrl Pts',(72.6087663095547,-2.58807004568195,340.323024123761));
#15235=CARTESIAN_POINT('Ctrl Pts',(72.60135731617,-2.4447723494503,340.388044053445));
#15236=CARTESIAN_POINT('Ctrl Pts',(72.5939437585897,-2.301386376895,340.453104037648));
#15237=CARTESIAN_POINT('Ctrl Pts',(72.5865302010096,-2.15552999179425,340.51237817974));
#15238=CARTESIAN_POINT('Ctrl Pts',(72.5791166434294,-2.00771576807876,340.565699233439));
#15239=CARTESIAN_POINT('Ctrl Pts',(72.5716925312927,-1.8596911037548,340.61909619942));
#15240=CARTESIAN_POINT('Ctrl Pts',(72.5642684191561,-1.70970338882277,340.6665230379));
#15241=CARTESIAN_POINT('Ctrl Pts',(72.5568443070194,-1.55827857792387,340.707862860658));
#15242=CARTESIAN_POINT('Ctrl Pts',(72.5529871818643,-1.47960729218889,340.729340562953));
#15243=CARTESIAN_POINT('Ctrl Pts',(72.5491300567091,-1.40054825221413,340.749176091258));
#15244=CARTESIAN_POINT('Ctrl Pts',(72.545272931554,-1.32117590016515,340.76735856379));
#15245=CARTESIAN_POINT('Ctrl Pts',(72.537848954116,-1.16840446363898,340.802355163696));
#15246=CARTESIAN_POINT('Ctrl Pts',(72.530424976678,-1.01401106733166,340.831330226838));
#15247=CARTESIAN_POINT('Ctrl Pts',(72.52300099924,-0.858511642384867,340.854134293163));
#15248=CARTESIAN_POINT('Ctrl Pts',(72.5155857832123,-0.703195730155659,
340.87691144726));
#15249=CARTESIAN_POINT('Ctrl Pts',(72.5081705671848,-0.546776753138711,
340.893532047254));
#15250=CARTESIAN_POINT('Ctrl Pts',(72.5007553511572,-0.389783708609473,
340.903896952268));
#15251=CARTESIAN_POINT('Ctrl Pts',(72.493347270013,-0.232941721997103,340.914251884223));
#15252=CARTESIAN_POINT('Ctrl Pts',(72.4859391888689,-0.0755271374395719,
340.918363079876));
#15253=CARTESIAN_POINT('Ctrl Pts',(72.4785311077248,0.0819231013680721,
340.916182820701));
#15254=CARTESIAN_POINT('Ctrl Pts',(72.4711285405508,0.239256147087246,340.914004184333));
#15255=CARTESIAN_POINT('Ctrl Pts',(72.4637259733768,0.39662442263823,340.905543422509));
#15256=CARTESIAN_POINT('Ctrl Pts',(72.4563234062028,0.553488244498939,340.890804811374));
#15257=CARTESIAN_POINT('Ctrl Pts',(72.4489247364481,0.710269478243119,340.876073960053));
#15258=CARTESIAN_POINT('Ctrl Pts',(72.4415260666933,0.86654641660166,340.855071876868));
#15259=CARTESIAN_POINT('Ctrl Pts',(72.4341273969386,1.02178187438646,340.827854868103));
#15260=CARTESIAN_POINT('Ctrl Pts',(72.4267299477346,1.17699172314103,340.8006423493));
#15261=CARTESIAN_POINT('Ctrl Pts',(72.4193324985307,1.33116006506648,340.767217004133));
#15262=CARTESIAN_POINT('Ctrl Pts',(72.4119350493267,1.48375719980413,340.727686717561));
#15263=CARTESIAN_POINT('Ctrl Pts',(72.4045379208632,1.63634771819606,340.688158144954));
#15264=CARTESIAN_POINT('Ctrl Pts',(72.3971407923998,1.78736680356902,340.642525250844));
#15265=CARTESIAN_POINT('Ctrl Pts',(72.3897436639363,1.93629753769941,340.590946467996));
#15266=CARTESIAN_POINT('Ctrl Pts',(72.3823453964997,2.08525120344516,340.539359743304));
#15267=CARTESIAN_POINT('Ctrl Pts',(72.3749471290631,2.23211552501007,340.4818254291));
#15268=CARTESIAN_POINT('Ctrl Pts',(72.3675488616265,2.3763914079367,340.418550953787));
#15269=CARTESIAN_POINT('Ctrl Pts',(72.3601479951008,2.52071797649814,340.355254249485));
#15270=CARTESIAN_POINT('Ctrl Pts',(72.352747128575,2.66245395434451,340.28621351887));
#15271=CARTESIAN_POINT('Ctrl Pts',(72.3453462620492,2.801122923585,340.211683118674));
#15272=CARTESIAN_POINT('Ctrl Pts',(72.3379372686645,2.93994416461109,340.137070876973));
#15273=CARTESIAN_POINT('Ctrl Pts',(72.3305282752798,3.07569134228388,340.056957103882));
#15274=CARTESIAN_POINT('Ctrl Pts',(72.323119281895,3.20791459414548,339.971641028792));
#15275=CARTESIAN_POINT('Ctrl Pts',(72.3157057243148,3.3402193000911,339.886272396057));
#15276=CARTESIAN_POINT('Ctrl Pts',(72.3082921667346,3.46899544995079,339.795695289551));
#15277=CARTESIAN_POINT('Ctrl Pts',(72.3008786091543,3.59382501959234,339.700250237067));
#15278=CARTESIAN_POINT('Ctrl Pts',(72.2934544970176,3.71883230697929,339.604669301078));
#15279=CARTESIAN_POINT('Ctrl Pts',(72.2860303848809,3.83988150610707,339.504206815396));
#15280=CARTESIAN_POINT('Ctrl Pts',(72.2786062727442,3.95658969894248,339.399241811576));
#15281=CARTESIAN_POINT('Ctrl Pts',(72.2747491475896,4.01722430386967,339.344708266132));
#15282=CARTESIAN_POINT('Ctrl Pts',(72.2708920224349,4.07668780572416,339.288959975301));
#15283=CARTESIAN_POINT('Ctrl Pts',(72.2670348972802,4.13493076885349,339.232053650332));
#15284=CARTESIAN_POINT('Ctrl Pts',(72.2596109198422,4.24703354666201,339.122523558435));
#15285=CARTESIAN_POINT('Ctrl Pts',(72.2521869424042,4.35495042124674,339.008370926896));
#15286=CARTESIAN_POINT('Ctrl Pts',(72.2447629649662,4.45827650851751,338.889948731809));
#15287=CARTESIAN_POINT('Ctrl Pts',(72.2373477489385,4.56148065545912,338.77166629273));
#15288=CARTESIAN_POINT('Ctrl Pts',(72.2299325329109,4.66010455636274,338.64912459825));
#15289=CARTESIAN_POINT('Ctrl Pts',(72.2225173168832,4.75377857076852,338.522714842647));
#15290=CARTESIAN_POINT('Ctrl Pts',(72.2151092357391,4.84736245250915,338.396426717873));
#15291=CARTESIAN_POINT('Ctrl Pts',(72.207701154595,4.93600570879356,338.266278239294));
#15292=CARTESIAN_POINT('Ctrl Pts',(72.2002930734509,5.01937764105134,338.132695111085));
#15293=CARTESIAN_POINT('Ctrl Pts',(72.1928905062769,5.10268751805733,337.999211411237));
#15294=CARTESIAN_POINT('Ctrl Pts',(72.1854879391029,5.18073368662685,337.862298467319));
#15295=CARTESIAN_POINT('Ctrl Pts',(72.1780853719288,5.25322768894203,337.722412424787));
#15296=CARTESIAN_POINT('Ctrl Pts',(72.1706867021741,5.32568352348182,337.582600031644));
#15297=CARTESIAN_POINT('Ctrl Pts',(72.1632880324193,5.3925928421868,337.439817987846));
#15298=CARTESIAN_POINT('Ctrl Pts',(72.1558893626645,5.45371229248286,337.294548494437));
#15299=CARTESIAN_POINT('Ctrl Pts',(72.1484919134605,5.51482165996753,337.149302965983));
#15300=CARTESIAN_POINT('Ctrl Pts',(72.1410944642566,5.57014291011179,337.001571146005));
#15301=CARTESIAN_POINT('Ctrl Pts',(72.1336970150526,5.61948011442046,336.851856853575));
#15302=CARTESIAN_POINT('Ctrl Pts',(72.1262998865891,5.66881517955393,336.702149052496));
#15303=CARTESIAN_POINT('Ctrl Pts',(72.1189027581256,5.71216659792967,336.550459304337));
#15304=CARTESIAN_POINT('Ctrl Pts',(72.1115056296621,5.74938786492976,336.39730803372));
#15305=CARTESIAN_POINT('Ctrl Pts',(72.1041073622255,5.78661486307582,336.24413318163));
#15306=CARTESIAN_POINT('Ctrl Pts',(72.0967090947889,5.81770974229293,336.08949672168));
#15307=CARTESIAN_POINT('Ctrl Pts',(72.0893108273523,5.84257684490011,335.933930604455));
#15308=CARTESIAN_POINT('Ctrl Pts',(72.0819099608265,5.86745268358196,335.778309835217));
#15309=CARTESIAN_POINT('Ctrl Pts',(72.0745090943007,5.88609633070922,335.621759126749));
#15310=CARTESIAN_POINT('Ctrl Pts',(72.0671082277749,5.89846386322769,335.464816756042));
#15311=CARTESIAN_POINT('Ctrl Pts',(72.0596992343901,5.91084497647925,335.307702047607));
#15312=CARTESIAN_POINT('Ctrl Pts',(72.0522902410054,5.91693618254478,335.150195190316));
#15313=CARTESIAN_POINT('Ctrl Pts',(72.0448812476206,5.91674566341376,334.9928364133));
#15314=CARTESIAN_POINT('Ctrl Pts',(72.0374676900403,5.9165550269164,334.835380697849));
#15315=CARTESIAN_POINT('Ctrl Pts',(72.0300541324601,5.91007496954033,334.678073616469));
#15316=CARTESIAN_POINT('Ctrl Pts',(72.0226405748798,5.89736563152799,334.5214509737));
#15317=CARTESIAN_POINT('Ctrl Pts',(72.0152164627431,5.88463819944623,334.364605349926));
#15318=CARTESIAN_POINT('Ctrl Pts',(72.0077923506064,5.8656638194122,334.208446480369));
#15319=CARTESIAN_POINT('Ctrl Pts',(72.0003682384697,5.84055400822791,334.053501484696));
#15320=CARTESIAN_POINT('Ctrl Pts',(71.9965111133152,5.82750845038064,333.973001321259));
#15321=CARTESIAN_POINT('Ctrl Pts',(71.9926539881607,5.8128076361528,333.892828594951));
#15322=CARTESIAN_POINT('Ctrl Pts',(71.9887968630062,5.7964725027736,333.813055566975));
#15323=CARTESIAN_POINT('Ctrl Pts',(71.9813728855682,5.76503155730365,333.659512931947));
#15324=CARTESIAN_POINT('Ctrl Pts',(71.9739489081302,5.72743818720968,333.506988790802));
#15325=CARTESIAN_POINT('Ctrl Pts',(71.9665249306922,5.68377011160646,333.356014634825));
#15326=CARTESIAN_POINT('Ctrl Pts',(71.9591097146646,5.64015357090266,333.205218651068));
#15327=CARTESIAN_POINT('Ctrl Pts',(71.951694498637,5.59047669751993,333.055969366426));
#15328=CARTESIAN_POINT('Ctrl Pts',(71.9442792826093,5.53486842140816,332.908789317118));
#15329=CARTESIAN_POINT('Ctrl Pts',(71.9368712014653,5.47931365129966,332.761750883713));
#15330=CARTESIAN_POINT('Ctrl Pts',(71.9294631203212,5.41783897139126,332.616778068705));
#15331=CARTESIAN_POINT('Ctrl Pts',(71.9220550391771,5.35062340543414,332.474379336535));
#15332=CARTESIAN_POINT('Ctrl Pts',(71.9146524720031,5.28345786925032,332.332086594342));
#15333=CARTESIAN_POINT('Ctrl Pts',(71.9072499048291,5.21056011390173,332.192364456133));
#15334=CARTESIAN_POINT('Ctrl Pts',(71.8998473376551,5.13215762075654,332.055702338721));
#15335=CARTESIAN_POINT('Ctrl Pts',(71.8924486679004,5.05379640618144,331.919112173317));
#15336=CARTESIAN_POINT('Ctrl Pts',(71.8850499981457,4.96993641103757,331.78557914304));
#15337=CARTESIAN_POINT('Ctrl Pts',(71.877651328391,4.88085143643022,331.655568834914));
#15338=CARTESIAN_POINT('Ctrl Pts',(71.870253879187,4.79178115807731,331.525579974453));
#15339=CARTESIAN_POINT('Ctrl Pts',(71.862856429983,4.69748782172357,331.399112990339));
#15340=CARTESIAN_POINT('Ctrl Pts',(71.8554589807791,4.59828907142544,331.276605288435));
#15341=CARTESIAN_POINT('Ctrl Pts',(71.8480618523156,4.49909462221226,331.154102898252));
#15342=CARTESIAN_POINT('Ctrl Pts',(71.8406647238522,4.39499541681371,331.035559738993));
#15343=CARTESIAN_POINT('Ctrl Pts',(71.8332675953887,4.286349809343,330.921380641143));
#15344=CARTESIAN_POINT('Ctrl Pts',(71.8258693279521,4.17768747316082,330.807183962562));
#15345=CARTESIAN_POINT('Ctrl Pts',(71.8184710605155,4.06447759833277,330.697352953731));
#15346=CARTESIAN_POINT('Ctrl Pts',(71.8110727930789,3.94711574759629,330.59225592422));
#15347=CARTESIAN_POINT('Ctrl Pts',(71.8036719265532,3.82971266640744,330.487121973017));
#15348=CARTESIAN_POINT('Ctrl Pts',(71.7962710600275,3.70815498302717,330.386725561173));
#15349=CARTESIAN_POINT('Ctrl Pts',(71.7888701935017,3.58287157677643,330.291394917088));
#15350=CARTESIAN_POINT('Ctrl Pts',(71.781461200117,3.45745059736798,330.195959590841));
#15351=CARTESIAN_POINT('Ctrl Pts',(71.7740522067323,3.32829602192653,330.105601367489));
#15352=CARTESIAN_POINT('Ctrl Pts',(71.7666432133475,3.19586656839799,330.020605715602));
#15353=CARTESIAN_POINT('Ctrl Pts',(71.7592296557673,3.06335553375799,329.935557703462));
#15354=CARTESIAN_POINT('Ctrl Pts',(71.7518160981871,2.92756592215524,329.855879033942));
#15355=CARTESIAN_POINT('Ctrl Pts',(71.7444025406068,2.78898084839398,329.781809088411));
#15356=CARTESIAN_POINT('Ctrl Pts',(71.7369784284702,2.65019847340903,329.707633690752));
#15357=CARTESIAN_POINT('Ctrl Pts',(71.7295543163335,2.50861302270973,329.639083127011));
#15358=CARTESIAN_POINT('Ctrl Pts',(71.7221302041968,2.36472811061008,329.57634887503));
#15359=CARTESIAN_POINT('Ctrl Pts',(71.718273079042,2.28997410586941,329.543755905401));
#15360=CARTESIAN_POINT('Ctrl Pts',(71.7144159538872,2.21459969578901,329.512732071195));
#15361=CARTESIAN_POINT('Ctrl Pts',(71.7105588287323,2.13867697669353,329.483298870533));
#15362=CARTESIAN_POINT('Ctrl Pts',(71.7031348512943,1.99254519953525,329.426647502254));
#15363=CARTESIAN_POINT('Ctrl Pts',(71.6957108738563,1.84394046562048,329.375721004578));
#15364=CARTESIAN_POINT('Ctrl Pts',(71.6882868964183,1.69335177558446,329.330741642276));
#15365=CARTESIAN_POINT('Ctrl Pts',(71.6808716803907,1.54294080285997,329.285815362389));
#15366=CARTESIAN_POINT('Ctrl Pts',(71.673456464363,1.39055088866465,329.246822353184));
#15367=CARTESIAN_POINT('Ctrl Pts',(71.6660412483354,1.23669121624611,329.213936969047));
#15368=CARTESIAN_POINT('Ctrl Pts',(71.6586331671913,1.08297958682957,329.181083227061));
#15369=CARTESIAN_POINT('Ctrl Pts',(71.6512250860472,0.927801377115052,329.154325488162));
#15370=CARTESIAN_POINT('Ctrl Pts',(71.6438170049031,0.771681045721263,329.133788366742));
#15371=CARTESIAN_POINT('Ctrl Pts',(71.6364144377291,0.615676917541566,329.113266531476));
#15372=CARTESIAN_POINT('Ctrl Pts',(71.629011870555,0.458732432388857,329.098956142915));
#15373=CARTESIAN_POINT('Ctrl Pts',(71.621609303381,0.301382254523396,329.090930758642));
#15374=CARTESIAN_POINT('Ctrl Pts',(71.6142106336263,0.144114920838886,329.0829095997));
#15375=CARTESIAN_POINT('Ctrl Pts',(71.6068119638716,-0.0135573083823089,
329.081166873884));
#15376=CARTESIAN_POINT('Ctrl Pts',(71.5994132941168,-0.17109474158854,329.085724291859));
#15377=CARTESIAN_POINT('Ctrl Pts',(71.5920158449128,-0.328606186010314,
329.090280958003));
#15378=CARTESIAN_POINT('Ctrl Pts',(71.5846183957088,-0.485982505858217,
329.101135694425));
#15379=CARTESIAN_POINT('Ctrl Pts',(71.5772209465048,-0.642683981786378,
329.118258092873));
#15380=CARTESIAN_POINT('Ctrl Pts',(71.5698238180413,-0.799378663411509,
329.135379748923));
#15381=CARTESIAN_POINT('Ctrl Pts',(71.5624266895779,-0.955398188292443,
329.158768486122));
#15382=CARTESIAN_POINT('Ctrl Pts',(71.5550295611144,-1.11020819986524,329.188342033855));
#15383=CARTESIAN_POINT('Ctrl Pts',(71.5476312936778,-1.26504204831536,329.217920135176));
#15384=CARTESIAN_POINT('Ctrl Pts',(71.5402330262411,-1.41866564603453,329.253684873166));
#15385=CARTESIAN_POINT('Ctrl Pts',(71.5328347588045,-1.57055521195258,329.295502924121));
#15386=CARTESIAN_POINT('Ctrl Pts',(71.5254338922787,-1.72249813827276,329.337335666198));
#15387=CARTESIAN_POINT('Ctrl Pts',(71.518033025753,-1.87270546031198,329.385225856279));
#15388=CARTESIAN_POINT('Ctrl Pts',(71.5106321592272,-2.02066907259672,329.438990463814));
#15389=CARTESIAN_POINT('Ctrl Pts',(71.5032231658424,-2.16879516307341,329.492814110029));
#15390=CARTESIAN_POINT('Ctrl Pts',(71.4958141724577,-2.31467227245839,329.5525249285));
#15391=CARTESIAN_POINT('Ctrl Pts',(71.4884051790729,-2.45781210553765,329.617891656946));
#15392=CARTESIAN_POINT('Ctrl Pts',(71.4809916214926,-2.60104011769161,329.683298653551));
#15393=CARTESIAN_POINT('Ctrl Pts',(71.4735780639124,-2.74152716120539,329.754368334855));
#15394=CARTESIAN_POINT('Ctrl Pts',(71.4661645063321,-2.87881049403801,329.830823982305));
#15395=CARTESIAN_POINT('Ctrl Pts',(71.4587403941954,-3.01628927482789,329.907388478366));
#15396=CARTESIAN_POINT('Ctrl Pts',(71.4513162820587,-3.15055491788447,329.989354060982));
#15397=CARTESIAN_POINT('Ctrl Pts',(71.443892169922,-3.2811738708044,330.07640084978));
#15398=CARTESIAN_POINT('Ctrl Pts',(71.4400350447674,-3.34903567564968,330.12162516112));
#15399=CARTESIAN_POINT('Ctrl Pts',(71.4361779196129,-3.41591369797062,330.16822033376));
#15400=CARTESIAN_POINT('Ctrl Pts',(71.4323207944583,-3.48175084408011,330.216137374229));
#15401=CARTESIAN_POINT('Ctrl Pts',(71.4249601178028,-3.60738999889424,330.30757901199));
#15402=CARTESIAN_POINT('Ctrl Pts',(71.4175994411473,-3.72962979400118,330.404123189567));
#15403=CARTESIAN_POINT('Ctrl Pts',(71.4102387644918,-3.84802294240781,330.505486678493));
#15404=CARTESIAN_POINT('Ctrl Pts',(71.4028868057498,-3.96627586712788,330.606730113495));
#15405=CARTESIAN_POINT('Ctrl Pts',(71.3955348470077,-4.08069092514987,330.712781256849));
#15406=CARTESIAN_POINT('Ctrl Pts',(71.3881828882656,-4.19084984256576,330.823313734602));
#15407=CARTESIAN_POINT('Ctrl Pts',(71.3808379650751,-4.30090334198744,330.933740436877));
#15408=CARTESIAN_POINT('Ctrl Pts',(71.3734930418846,-4.40670854038181,331.048639671035));
#15409=CARTESIAN_POINT('Ctrl Pts',(71.3661481186941,-4.50788046984098,331.167645080094));
#15410=CARTESIAN_POINT('Ctrl Pts',(71.3588085550214,-4.60897857514308,331.286563652083));
#15411=CARTESIAN_POINT('Ctrl Pts',(71.3514689913487,-4.70544989620773,331.409582146164));
#15412=CARTESIAN_POINT('Ctrl Pts',(71.3441294276761,-4.79694671114355,331.536297816938));
#15413=CARTESIAN_POINT('Ctrl Pts',(71.3367930035454,-4.88840438777385,331.662959284331));
#15414=CARTESIAN_POINT('Ctrl Pts',(71.3294565794146,-4.97489156949275,331.793314474467));
#15415=CARTESIAN_POINT('Ctrl Pts',(71.3221201552839,-5.05610125657842,331.926928141789));
#15416=CARTESIAN_POINT('Ctrl Pts',(71.3147852802572,-5.13729379603809,332.060513596256));
#15417=CARTESIAN_POINT('Ctrl Pts',(71.3074504052306,-5.21321086032108,332.197355834426));
#15418=CARTESIAN_POINT('Ctrl Pts',(71.3001155302039,-5.28358931096442,332.336991446585));
#15419=CARTESIAN_POINT('Ctrl Pts',(71.292780694991,-5.35396737959323,332.476626300801));
#15420=CARTESIAN_POINT('Ctrl Pts',(71.2854458597781,-5.41880672313075,332.619054159305));
#15421=CARTESIAN_POINT('Ctrl Pts',(71.2781110245651,-5.47789073763026,332.763788107293));
#15422=CARTESIAN_POINT('Ctrl Pts',(71.2707747201294,-5.53698658710326,332.908551046582));
#15423=CARTESIAN_POINT('Ctrl Pts',(71.2634384156937,-5.59032466976917,333.055620642552));
#15424=CARTESIAN_POINT('Ctrl Pts',(71.256102111258,-5.63773708135723,333.204491391279));
#15425=CARTESIAN_POINT('Ctrl Pts',(71.248758650777,-5.68519574039464,333.353507352878));
#15426=CARTESIAN_POINT('Ctrl Pts',(71.2414151902958,-5.72671706718547,333.504327613786));
#15427=CARTESIAN_POINT('Ctrl Pts',(71.2340717298148,-5.76218330324322,333.656432308246));
#15428=CARTESIAN_POINT('Ctrl Pts',(71.2267246167017,-5.79766718018159,333.808612659473));
#15429=CARTESIAN_POINT('Ctrl Pts',(71.2193775035886,-5.82708989440807,333.962078343988));
#15430=CARTESIAN_POINT('Ctrl Pts',(71.2120303904755,-5.85038523797935,334.116301448607));
#15431=CARTESIAN_POINT('Ctrl Pts',(71.2046724631652,-5.87371486990786,334.270751553824));
#15432=CARTESIAN_POINT('Ctrl Pts',(71.1973145358549,-5.89089906999728,334.425960928768));
#15433=CARTESIAN_POINT('Ctrl Pts',(71.1899566085446,-5.90192364540613,334.581397746905));
#15434=CARTESIAN_POINT('Ctrl Pts',(71.1833217405976,-5.91186484201282,334.721559876667));
#15435=CARTESIAN_POINT('Ctrl Pts',(71.1766868726506,-5.91679822761007,334.861906730318));
#15436=CARTESIAN_POINT('Ctrl Pts',(71.1700520047036,-5.91674964447282,335.002051129139));
#15437=CARTESIAN_POINT('',(69.4200520047036,-5.91677564200862,334.994557387791));
#15438=CARTESIAN_POINT('Ctrl Pts',(71.1700520047036,-5.92563727779681,335.002054210169));
#15439=CARTESIAN_POINT('Ctrl Pts',(71.1647289231972,-5.92614260361302,335.114659599285));
#15440=CARTESIAN_POINT('Ctrl Pts',(71.1594058416908,-5.92321159438174,335.227238160444));
#15441=CARTESIAN_POINT('Ctrl Pts',(71.0613367487598,-5.80437581181731,337.297592947633));
#15442=CARTESIAN_POINT('Ctrl Pts',(70.8758447259104,-3.44289158951305,341.090904729519));
#15443=CARTESIAN_POINT('Ctrl Pts',(70.5976066916366,3.25882553864336,341.191339033676));
#15444=CARTESIAN_POINT('Ctrl Pts',(70.3193686573626,6.96996657017265,335.610072890641));
#15445=CARTESIAN_POINT('Ctrl Pts',(70.0411306230885,4.28487215679163,329.468951860526));
#15446=CARTESIAN_POINT('Ctrl Pts',(69.7628925888149,-2.33238619026497,328.403592069872));
#15447=CARTESIAN_POINT('Ctrl Pts',(69.5558663826863,-5.66344677170153,332.11502018656));
#15448=CARTESIAN_POINT('Ctrl Pts',(69.4415861879827,-5.92099704865869,334.537243699616));
#15449=CARTESIAN_POINT('Ctrl Pts',(69.4200520047036,-5.91677564200862,334.994557387791));
#15450=CARTESIAN_POINT('',(67.6700520047036,-5.90704436558369,335.000708871167));
#15451=CARTESIAN_POINT('Ctrl Pts',(69.4200520047036,-5.91677564200862,334.994557387791));
#15452=CARTESIAN_POINT('Ctrl Pts',(69.348840176558,-5.90281578660099,336.5068573134));
#15453=CARTESIAN_POINT('Ctrl Pts',(69.1848823369878,-4.54245475610646,340.011087696333));
#15454=CARTESIAN_POINT('Ctrl Pts',(68.9281784859928,1.35723518751296,341.863711500856));
#15455=CARTESIAN_POINT('Ctrl Pts',(68.649940451719,6.50631927003558,337.573020108275));
#15456=CARTESIAN_POINT('Ctrl Pts',(68.371702417445,5.6846501915613,330.92110614004));
#15457=CARTESIAN_POINT('Ctrl Pts',(68.0934643831711,-0.353738462407954,
328.012332862722));
#15458=CARTESIAN_POINT('Ctrl Pts',(67.8595809122574,-5.15666167148477,330.957504813185));
#15459=CARTESIAN_POINT('Ctrl Pts',(67.7184434527681,-5.90594384398274,333.968760031375));
#15460=CARTESIAN_POINT('Ctrl Pts',(67.6700520047036,-5.90704436558369,335.000708871167));
#15461=CARTESIAN_POINT('',(65.9200528093559,-5.91850530180183,335.005138733431));
#15462=CARTESIAN_POINT('Ctrl Pts',(67.6700520047036,-5.90704436558369,335.000708871167));
#15463=CARTESIAN_POINT('Ctrl Pts',(67.6256974413435,-5.90805308007831,335.946571043714));
#15464=CARTESIAN_POINT('Ctrl Pts',(67.4885968665589,-5.24689642131051,338.86891281132));
#15465=CARTESIAN_POINT('Ctrl Pts',(67.2587502803491,-0.657146055416641,
341.965686038222));
#15466=CARTESIAN_POINT('Ctrl Pts',(66.9805122460754,5.5019745583164,339.322140543857));
#15467=CARTESIAN_POINT('Ctrl Pts',(66.7022742118012,6.61201432889349,332.712230467085));
#15468=CARTESIAN_POINT('Ctrl Pts',(66.4240361775276,1.65430614301727,328.201772723248));
#15469=CARTESIAN_POINT('Ctrl Pts',(66.1632958442427,-4.41428479853386,329.82126715782));
#15470=CARTESIAN_POINT('Ctrl Pts',(65.9953015223826,-5.90475744606087,333.408917292735));
#15471=CARTESIAN_POINT('Ctrl Pts',(65.9200532119472,-5.91938465457413,335.005130959516));
#15472=CARTESIAN_POINT('',(64.1700505935735,-5.92083642894063,334.996626893551));
#15473=CARTESIAN_POINT('Ctrl Pts',(65.9200520047037,-5.91674775497404,335.005154271017));
#15474=CARTESIAN_POINT('Ctrl Pts',(65.9090739000334,-5.91654498274101,335.237922813964));
#15475=CARTESIAN_POINT('Ctrl Pts',(65.898095795363,-5.90260318783092,335.470115853266));
#15476=CARTESIAN_POINT('Ctrl Pts',(65.8871176906927,-5.87514389833077,335.700438959801));
#15477=CARTESIAN_POINT('Ctrl Pts',(65.8805984967883,-5.8588375833427,335.837213115016));
#15478=CARTESIAN_POINT('Ctrl Pts',(65.874079302884,-5.83776526405744,335.973328646159));
#15479=CARTESIAN_POINT('Ctrl Pts',(65.8675601089796,-5.81198034837483,336.108519279311));
#15480=CARTESIAN_POINT('Ctrl Pts',(65.8601361315416,-5.78261680510881,336.262472701327));
#15481=CARTESIAN_POINT('Ctrl Pts',(65.8527121541035,-5.74708763781901,336.41549084855));
#15482=CARTESIAN_POINT('Ctrl Pts',(65.8452881766655,-5.70546337748581,336.567041228133));
#15483=CARTESIAN_POINT('Ctrl Pts',(65.8378729606378,-5.66388824004251,336.718412755466));
#15484=CARTESIAN_POINT('Ctrl Pts',(65.8304577446101,-5.61623242547244,336.868319606721));
#15485=CARTESIAN_POINT('Ctrl Pts',(65.8230425285825,-5.5626177919096,337.016237551389));
#15486=CARTESIAN_POINT('Ctrl Pts',(65.8156344474383,-5.50905474607722,337.164013170155));
#15487=CARTESIAN_POINT('Ctrl Pts',(65.8082263662942,-5.44954442200096,337.309803343657));
#15488=CARTESIAN_POINT('Ctrl Pts',(65.80081828515,-5.38425895716904,337.453097235057));
#15489=CARTESIAN_POINT('Ctrl Pts',(65.793415717976,-5.31902208550095,337.596284470197));
#15490=CARTESIAN_POINT('Ctrl Pts',(65.786013150802,-5.24801878617323,337.736978784671));
#15491=CARTESIAN_POINT('Ctrl Pts',(65.7786105836279,-5.17146990722256,337.874687732814));
#15492=CARTESIAN_POINT('Ctrl Pts',(65.7712119138731,-5.09496133092188,338.012324177798));
#15493=CARTESIAN_POINT('Ctrl Pts',(65.7638132441183,-5.0129131706709,338.146978061368));
#15494=CARTESIAN_POINT('Ctrl Pts',(65.7564145743635,-4.92559291198239,338.27818013964));
#15495=CARTESIAN_POINT('Ctrl Pts',(65.7490171251595,-4.83828705842531,338.409360573642));
#15496=CARTESIAN_POINT('Ctrl Pts',(65.7416196759555,-4.74571103914577,338.537090022111));
#15497=CARTESIAN_POINT('Ctrl Pts',(65.7342222267515,-4.64817655936471,338.660926827386));
#15498=CARTESIAN_POINT('Ctrl Pts',(65.7268250982879,-4.55064630850865,338.784758263312));
#15499=CARTESIAN_POINT('Ctrl Pts',(65.7194279698244,-4.44815825554298,338.904697098438));
#15500=CARTESIAN_POINT('Ctrl Pts',(65.7120308413609,-4.3410652521591,339.020333697468));
#15501=CARTESIAN_POINT('Ctrl Pts',(65.7046325739243,-4.23395575912603,339.135988101647));
#15502=CARTESIAN_POINT('Ctrl Pts',(65.6972343064876,-4.12224015747432,339.247338676892));
#15503=CARTESIAN_POINT('Ctrl Pts',(65.689836039051,-4.00630899756151,339.354011802758));
#15504=CARTESIAN_POINT('Ctrl Pts',(65.6824351725252,-3.89033710981307,339.460722404015));
#15505=CARTESIAN_POINT('Ctrl Pts',(65.6750343059994,-3.77014698966021,339.562752031663));
#15506=CARTESIAN_POINT('Ctrl Pts',(65.6676334394736,-3.64616304254419,339.659766692624));
#15507=CARTESIAN_POINT('Ctrl Pts',(65.6602244460888,-3.52204294920091,339.756887884958));
#15508=CARTESIAN_POINT('Ctrl Pts',(65.652815452704,-3.3941210033003,339.848982882879));
#15509=CARTESIAN_POINT('Ctrl Pts',(65.6454064593192,-3.26285202391792,339.935760046084));
#15510=CARTESIAN_POINT('Ctrl Pts',(65.6379929017389,-3.13150217831639,340.022590667013));
#15511=CARTESIAN_POINT('Ctrl Pts',(65.6305793441586,-2.99680150920922,340.104096732665));
#15512=CARTESIAN_POINT('Ctrl Pts',(65.6231657865784,-2.85922985299295,340.180032356101));
#15513=CARTESIAN_POINT('Ctrl Pts',(65.6157416744416,-2.72146233833811,340.256076087799));
#15514=CARTESIAN_POINT('Ctrl Pts',(65.6083175623049,-2.58081600605014,340.326533371689));
#15515=CARTESIAN_POINT('Ctrl Pts',(65.6008934501681,-2.43779183739425,340.391205943018));
#15516=CARTESIAN_POINT('Ctrl Pts',(65.597036325014,-2.36348502354024,340.424805947579));
#15517=CARTESIAN_POINT('Ctrl Pts',(65.5931791998598,-2.28853666020672,340.456845342317));
#15518=CARTESIAN_POINT('Ctrl Pts',(65.5893220747057,-2.21301854667385,340.487301656969));
#15519=CARTESIAN_POINT('Ctrl Pts',(65.5818980972677,-2.0676655315084,340.545922257491));
#15520=CARTESIAN_POINT('Ctrl Pts',(65.5744741198297,-1.91976243592748,340.598851922377));
#15521=CARTESIAN_POINT('Ctrl Pts',(65.5670501423917,-1.76979521288567,340.645861800199));
#15522=CARTESIAN_POINT('Ctrl Pts',(65.5596349263641,-1.62000497373084,340.692816199293));
#15523=CARTESIAN_POINT('Ctrl Pts',(65.5522197103365,-1.46815580863526,340.733864606996));
#15524=CARTESIAN_POINT('Ctrl Pts',(65.5448044943088,-1.31475449864639,340.768825805204));
#15525=CARTESIAN_POINT('Ctrl Pts',(65.5373964131647,-1.1615007906256,340.803753363924));
#15526=CARTESIAN_POINT('Ctrl Pts',(65.5299883320207,-1.00669827237262,340.832605291131));
#15527=CARTESIAN_POINT('Ctrl Pts',(65.5225802508766,-0.850869670954471,
340.855249897788));
#15528=CARTESIAN_POINT('Ctrl Pts',(65.5151776837026,-0.695157055610355,
340.877877649651));
#15529=CARTESIAN_POINT('Ctrl Pts',(65.5077751165286,-0.538420245553648,
340.894307227058));
#15530=CARTESIAN_POINT('Ctrl Pts',(65.5003725493546,-0.381192862395804,
340.904457855228));
#15531=CARTESIAN_POINT('Ctrl Pts',(65.4929738795998,-0.224048258768149,
340.914603139136));
#15532=CARTESIAN_POINT('Ctrl Pts',(65.4855752098451,-0.0664139679263883,
340.918476033599));
#15533=CARTESIAN_POINT('Ctrl Pts',(65.4781765400904,0.0911706611757941,
340.916047538098));
#15534=CARTESIAN_POINT('Ctrl Pts',(65.4707790908864,0.248729293707663,340.913619443224));
#15535=CARTESIAN_POINT('Ctrl Pts',(65.4633816416824,0.406237907955571,340.904892027271));
#15536=CARTESIAN_POINT('Ctrl Pts',(65.4559841924784,0.563156422989418,340.889888403505));
#15537=CARTESIAN_POINT('Ctrl Pts',(65.448587064015,0.720068134310021,340.874885430271));
#15538=CARTESIAN_POINT('Ctrl Pts',(65.4411899355515,0.876389425772367,340.853606825821));
#15539=CARTESIAN_POINT('Ctrl Pts',(65.433792807088,1.03158487802041,340.826127633509));
#15540=CARTESIAN_POINT('Ctrl Pts',(65.4263945396514,1.18680422649391,340.798644210087));
#15541=CARTESIAN_POINT('Ctrl Pts',(65.4189962722148,1.34089702307072,340.764958362871));
#15542=CARTESIAN_POINT('Ctrl Pts',(65.4115980047782,1.49333773313908,340.725196326527));
#15543=CARTESIAN_POINT('Ctrl Pts',(65.4041971382524,1.64583199723209,340.685420321362));
#15544=CARTESIAN_POINT('Ctrl Pts',(65.3967962717267,1.79667265834933,340.639563971162));
#15545=CARTESIAN_POINT('Ctrl Pts',(65.389395405201,1.94534918444987,340.587803424697));
#15546=CARTESIAN_POINT('Ctrl Pts',(65.3819864118162,2.0941889715901,340.535986040205));
#15547=CARTESIAN_POINT('Ctrl Pts',(65.3745774184314,2.24085952518916,340.478251634588));
#15548=CARTESIAN_POINT('Ctrl Pts',(65.3671684250467,2.38486946999285,340.414824851608));
#15549=CARTESIAN_POINT('Ctrl Pts',(65.3597548674665,2.52896812988996,340.351358995542));
#15550=CARTESIAN_POINT('Ctrl Pts',(65.3523413098862,2.67040258052837,340.28219393812));
#15551=CARTESIAN_POINT('Ctrl Pts',(65.344927752306,2.80870638332948,340.207600120472));
#15552=CARTESIAN_POINT('Ctrl Pts',(65.3375036401693,2.94720708691368,340.13290010487));
#15553=CARTESIAN_POINT('Ctrl Pts',(65.3300795280326,3.08256792076255,340.052756082643));
#15554=CARTESIAN_POINT('Ctrl Pts',(65.322655415896,3.21435105010636,339.967482047193));
#15555=CARTESIAN_POINT('Ctrl Pts',(65.3187982907412,3.28281769147805,339.923178752586));
#15556=CARTESIAN_POINT('Ctrl Pts',(65.3149411655864,3.35031916198981,339.877491429811));
#15557=CARTESIAN_POINT('Ctrl Pts',(65.3110840404317,3.41679771120956,339.830468296467));
#15558=CARTESIAN_POINT('Ctrl Pts',(65.3036600629937,3.54475188166431,339.739960815636));
#15559=CARTESIAN_POINT('Ctrl Pts',(65.2962360855557,3.66930041776815,339.644229225961));
#15560=CARTESIAN_POINT('Ctrl Pts',(65.2888121081177,3.78998789644607,339.54355833101));
#15561=CARTESIAN_POINT('Ctrl Pts',(65.2813968920901,3.91053294574074,339.443006242863));
#15562=CARTESIAN_POINT('Ctrl Pts',(65.2739816760624,4.0272257238441,339.337526689139));
#15563=CARTESIAN_POINT('Ctrl Pts',(65.2665664600348,4.13963959228238,339.22744776532));
#15564=CARTESIAN_POINT('Ctrl Pts',(65.2591583788907,4.25194529666245,339.117474758887));
#15565=CARTESIAN_POINT('Ctrl Pts',(65.2517502977467,4.35998002297345,339.002911452056));
#15566=CARTESIAN_POINT('Ctrl Pts',(65.2443422166026,4.46335015348345,338.884126152676));
#15567=CARTESIAN_POINT('Ctrl Pts',(65.2369396494286,4.56664334371741,338.765429267363));
#15568=CARTESIAN_POINT('Ctrl Pts',(65.2295370822546,4.66527860734633,338.642516927017));
#15569=CARTESIAN_POINT('Ctrl Pts',(65.2221345150806,4.75889924586057,338.515794153566));
#15570=CARTESIAN_POINT('Ctrl Pts',(65.2147358453258,4.85247059351786,338.389138099101));
#15571=CARTESIAN_POINT('Ctrl Pts',(65.2073371755711,4.94103235292452,338.258675906373));
#15572=CARTESIAN_POINT('Ctrl Pts',(65.1999385058164,5.02426826425997,338.124845431577));
#15573=CARTESIAN_POINT('Ctrl Pts',(65.1925410566124,5.10749044425467,337.991037034655));
#15574=CARTESIAN_POINT('Ctrl Pts',(65.1851436074084,5.18538832299996,337.853861775083));
#15575=CARTESIAN_POINT('Ctrl Pts',(65.1777461582045,5.25768906815454,337.713786326354));
#15576=CARTESIAN_POINT('Ctrl Pts',(65.170349029741,5.3299866784748,337.573716951053));
#15577=CARTESIAN_POINT('Ctrl Pts',(65.1629519012776,5.39668746655833,337.43074796826));
#15578=CARTESIAN_POINT('Ctrl Pts',(65.1555547728141,5.45756479182469,337.285370233799));
#15579=CARTESIAN_POINT('Ctrl Pts',(65.1481565053775,5.51845149067948,337.139970114796));
#15580=CARTESIAN_POINT('Ctrl Pts',(65.1407582379409,5.57351279717003,336.992160849907));
#15581=CARTESIAN_POINT('Ctrl Pts',(65.1333599705043,5.62257046778665,336.84245268522));
#15582=CARTESIAN_POINT('Ctrl Pts',(65.1259591039786,5.6716453728789,336.69269192648));
#15583=CARTESIAN_POINT('Ctrl Pts',(65.1185582374528,5.71471232665893,336.541031294172));
#15584=CARTESIAN_POINT('Ctrl Pts',(65.1111573709271,5.75164317820467,336.387995429788));
#15585=CARTESIAN_POINT('Ctrl Pts',(65.1037483775423,5.78861458335614,336.234791517394));
#15586=CARTESIAN_POINT('Ctrl Pts',(65.0963393841576,5.81943634247086,336.080209720115));
#15587=CARTESIAN_POINT('Ctrl Pts',(65.0889303907728,5.84403145193407,335.924784813514));
#15588=CARTESIAN_POINT('Ctrl Pts',(65.0815168331926,5.86864171283308,335.769264159809));
#15589=CARTESIAN_POINT('Ctrl Pts',(65.0741032756124,5.8870176372221,335.612899731633));
#15590=CARTESIAN_POINT('Ctrl Pts',(65.0666897180321,5.89913422813944,335.456230118354));
#15591=CARTESIAN_POINT('Ctrl Pts',(65.0592656058954,5.91126806924218,335.299337457199));
#15592=CARTESIAN_POINT('Ctrl Pts',(65.0518414937588,5.91712476535286,335.142139115129));
#15593=CARTESIAN_POINT('Ctrl Pts',(65.0444173816221,5.91673142270296,334.985173196588));
#15594=CARTESIAN_POINT('Ctrl Pts',(65.0405602564673,5.9165270653601,334.903623082353));
#15595=CARTESIAN_POINT('Ctrl Pts',(65.0367031313125,5.91463653986993,334.822135623827));
#15596=CARTESIAN_POINT('Ctrl Pts',(65.0328460061578,5.91106914136758,334.740785477892));
#15597=CARTESIAN_POINT('Ctrl Pts',(65.0254220287198,5.90420281348577,334.584207294977));
#15598=CARTESIAN_POINT('Ctrl Pts',(65.0179980512818,5.8911004368634,334.42766591759));
#15599=CARTESIAN_POINT('Ctrl Pts',(65.0105740738438,5.87175505333894,334.271698444263));
#15600=CARTESIAN_POINT('Ctrl Pts',(65.0031588578162,5.85243250027771,334.115915036021));
#15601=CARTESIAN_POINT('Ctrl Pts',(64.9957436417886,5.82688165130592,333.960704550447));
#15602=CARTESIAN_POINT('Ctrl Pts',(64.988328425761,5.79514753035372,333.806603308227));
#15603=CARTESIAN_POINT('Ctrl Pts',(64.9809203446168,5.76344394381292,333.652650341446));
#15604=CARTESIAN_POINT('Ctrl Pts',(64.9735122634727,5.7255690044362,333.499804856304));
#15605=CARTESIAN_POINT('Ctrl Pts',(64.9661041823286,5.68161942100958,333.348597166859));
#15606=CARTESIAN_POINT('Ctrl Pts',(64.9587016151547,5.63770255006059,333.197502024059));
#15607=CARTESIAN_POINT('Ctrl Pts',(64.9512990479807,5.58772014168348,333.048042606512));
#15608=CARTESIAN_POINT('Ctrl Pts',(64.9438964808067,5.53181975742786,332.900738050211));
#15609=CARTESIAN_POINT('Ctrl Pts',(64.9364978110519,5.47594880448024,332.753511049115));
#15610=CARTESIAN_POINT('Ctrl Pts',(64.9290991412972,5.41416621301346,332.608436997844));
#15611=CARTESIAN_POINT('Ctrl Pts',(64.9217004715424,5.34666903930941,332.466018795139));
#15612=CARTESIAN_POINT('Ctrl Pts',(64.9143030223384,5.27918300054306,332.323624087015));
#15613=CARTESIAN_POINT('Ctrl Pts',(64.9069055731345,5.20598441023189,332.183884694831));
#15614=CARTESIAN_POINT('Ctrl Pts',(64.8995081239305,5.12731805883598,332.047282592927));
#15615=CARTESIAN_POINT('Ctrl Pts',(64.892110995467,5.04865511827599,331.910686413852));
#15616=CARTESIAN_POINT('Ctrl Pts',(64.8847138670035,4.96452507425847,331.777227578006));
#15617=CARTESIAN_POINT('Ctrl Pts',(64.8773167385401,4.87521804969405,331.647362302539));
#15618=CARTESIAN_POINT('Ctrl Pts',(64.8699184711035,4.7858972740772,331.517477031062));
#15619=CARTESIAN_POINT('Ctrl Pts',(64.8625202036669,4.69139814221855,331.391186729227));
#15620=CARTESIAN_POINT('Ctrl Pts',(64.8551219362303,4.59205327314849,331.268917409241));
#15621=CARTESIAN_POINT('Ctrl Pts',(64.8477210697045,4.49267350318119,331.146605134757));
#15622=CARTESIAN_POINT('Ctrl Pts',(64.8403202031788,4.38844484180724,331.028316944103));
#15623=CARTESIAN_POINT('Ctrl Pts',(64.832919336653,4.27973912143312,330.914444515739));
#15624=CARTESIAN_POINT('Ctrl Pts',(64.8255103432683,4.17091403178527,330.800447044562));
#15625=CARTESIAN_POINT('Ctrl Pts',(64.8181013498835,4.05760232300439,330.69087528936));
#15626=CARTESIAN_POINT('Ctrl Pts',(64.8106923564988,3.94021202819587,330.586083401857));
#15627=CARTESIAN_POINT('Ctrl Pts',(64.8032787989186,3.82274941691652,330.481226958937));
#15628=CARTESIAN_POINT('Ctrl Pts',(64.7958652413383,3.70120350047246,330.381156487811));
#15629=CARTESIAN_POINT('Ctrl Pts',(64.7884516837581,3.57601366286169,330.286184470567));
#15630=CARTESIAN_POINT('Ctrl Pts',(64.7810275716214,3.45064559459811,330.191077243269));
#15631=CARTESIAN_POINT('Ctrl Pts',(64.7736034594847,3.32162354939444,330.101083179629));
#15632=CARTESIAN_POINT('Ctrl Pts',(64.766179347348,3.18941469949486,330.016470684631));
#15633=CARTESIAN_POINT('Ctrl Pts',(64.7623222221933,3.12072687915573,329.972511086923));
#15634=CARTESIAN_POINT('Ctrl Pts',(64.7584650970386,3.05117926500293,329.930003330584));
#15635=CARTESIAN_POINT('Ctrl Pts',(64.7546079718839,2.98083966773048,329.888980000256));
#15636=CARTESIAN_POINT('Ctrl Pts',(64.7471839944459,2.84545396926202,329.810020602629));
#15637=CARTESIAN_POINT('Ctrl Pts',(64.7397600170079,2.70672453754865,329.736325149011));
#15638=CARTESIAN_POINT('Ctrl Pts',(64.7323360395698,2.56509926474443,329.668190145503));
#15639=CARTESIAN_POINT('Ctrl Pts',(64.7249208235422,2.42364113107078,329.600135551551));
#15640=CARTESIAN_POINT('Ctrl Pts',(64.7175056075146,2.27929429199498,329.537628505835));
#15641=CARTESIAN_POINT('Ctrl Pts',(64.7100903914869,2.1325341160549,329.480921380669));
#15642=CARTESIAN_POINT('Ctrl Pts',(64.7026823103428,1.98591515201716,329.424268818812));
#15643=CARTESIAN_POINT('Ctrl Pts',(64.6952742291987,1.83688781978518,329.373405201078));
#15644=CARTESIAN_POINT('Ctrl Pts',(64.6878661480546,1.68595040643739,329.328536186351));
#15645=CARTESIAN_POINT('Ctrl Pts',(64.6804635808806,1.53512533856302,329.28370056845));
#15646=CARTESIAN_POINT('Ctrl Pts',(64.6730610137065,1.38239337660806,329.244850775169));
#15647=CARTESIAN_POINT('Ctrl Pts',(64.6656584465325,1.2282709271253,329.212143653123));
#15648=CARTESIAN_POINT('Ctrl Pts',(64.6582597767778,1.07422962243848,329.179453751235));
#15649=CARTESIAN_POINT('Ctrl Pts',(64.650861107023,0.918799652377362,329.152900156983));
#15650=CARTESIAN_POINT('Ctrl Pts',(64.6434624372682,0.762510553684954,329.132589308901));
#15651=CARTESIAN_POINT('Ctrl Pts',(64.6360649880642,0.606247237840906,329.112281811479));
#15652=CARTESIAN_POINT('Ctrl Pts',(64.6286675388603,0.449125444392178,329.09821506434));
#15653=CARTESIAN_POINT('Ctrl Pts',(64.6212700896563,0.291682946008149,329.090444041934));
#15654=CARTESIAN_POINT('Ctrl Pts',(64.6138729611928,0.134247274056367,329.082673356467));
#15655=CARTESIAN_POINT('Ctrl Pts',(64.6064758327293,-0.0235087024250638,
329.081197871375));
#15656=CARTESIAN_POINT('Ctrl Pts',(64.5990787042658,-0.181044338547331,
329.08602050139));
#15657=CARTESIAN_POINT('Ctrl Pts',(64.5916804368292,-0.338604231225055,
329.09084387397));
#15658=CARTESIAN_POINT('Ctrl Pts',(64.5842821693926,-0.495943342931435,
329.101967281142));
#15659=CARTESIAN_POINT('Ctrl Pts',(64.576883901956,-0.652523431670751,329.119341556116));
#15660=CARTESIAN_POINT('Ctrl Pts',(64.5694830354302,-0.809158528641985,
329.136721934856));
#15661=CARTESIAN_POINT('Ctrl Pts',(64.5620821689044,-0.96503370103994,329.160357512489));
#15662=CARTESIAN_POINT('Ctrl Pts',(64.5546813023786,-1.11961835824078,329.190147566901));
#15663=CARTESIAN_POINT('Ctrl Pts',(64.5472723089939,-1.2743727641742,329.21997033364));
#15664=CARTESIAN_POINT('Ctrl Pts',(64.5398633156091,-1.42783345818093,329.255961002987));
#15665=CARTESIAN_POINT('Ctrl Pts',(64.5324543222243,-1.57948181639369,329.29796810302));
#15666=CARTESIAN_POINT('Ctrl Pts',(64.525040764644,-1.73122359522613,329.340001080874));
#15667=CARTESIAN_POINT('Ctrl Pts',(64.5176272070638,-1.8811504589978,329.388057761112));
#15668=CARTESIAN_POINT('Ctrl Pts',(64.5102136494835,-2.02876185896069,329.441937758344));
#15669=CARTESIAN_POINT('Ctrl Pts',(64.5027895373468,-2.17658341077489,329.495894463615));
#15670=CARTESIAN_POINT('Ctrl Pts',(64.4953654252101,-2.32208257077187,329.555690902298));
#15671=CARTESIAN_POINT('Ctrl Pts',(64.4879413130734,-2.46478081776782,329.621079468623));
#15672=CARTESIAN_POINT('Ctrl Pts',(64.4840841879189,-2.53891830220502,329.655051461415));
#15673=CARTESIAN_POINT('Ctrl Pts',(64.4802270627644,-2.61230018603011,329.690532147838));
#15674=CARTESIAN_POINT('Ctrl Pts',(64.4763699376098,-2.68486237186319,329.727482137854));
#15675=CARTESIAN_POINT('Ctrl Pts',(64.4689459601718,-2.82452598372336,329.798601399278));
#15676=CARTESIAN_POINT('Ctrl Pts',(64.4615219827338,-2.96157251868736,329.875381099471));
#15677=CARTESIAN_POINT('Ctrl Pts',(64.4540980052958,-3.0955102583044,329.957605052831));
#15678=CARTESIAN_POINT('Ctrl Pts',(64.4466827892682,-3.22928993123667,330.039731969555));
#15679=CARTESIAN_POINT('Ctrl Pts',(64.4392675732405,-3.35996779675236,330.127290156948));
#15680=CARTESIAN_POINT('Ctrl Pts',(64.4318523572129,-3.48707438039661,330.220016440605));
#15681=CARTESIAN_POINT('Ctrl Pts',(64.4244442760688,-3.61405866272606,330.3126535035));
#15682=CARTESIAN_POINT('Ctrl Pts',(64.4170361949247,-3.73747820466366,330.410448544422));
#15683=CARTESIAN_POINT('Ctrl Pts',(64.4096281137806,-3.85689041153574,330.513093836963));
#15684=CARTESIAN_POINT('Ctrl Pts',(64.4022255466065,-3.97621373772126,330.615662728737));
#15685=CARTESIAN_POINT('Ctrl Pts',(64.3948229794325,-4.09153538608778,330.723074441593));
#15686=CARTESIAN_POINT('Ctrl Pts',(64.3874204122585,-4.20244400375068,330.834979596948));
#15687=CARTESIAN_POINT('Ctrl Pts',(64.3800217425037,-4.31329422851119,330.946825834728));
#15688=CARTESIAN_POINT('Ctrl Pts',(64.372623072749,-4.41973578778379,331.063160539011));
#15689=CARTESIAN_POINT('Ctrl Pts',(64.3652244029943,-4.52139261241745,331.18359601105));
#15690=CARTESIAN_POINT('Ctrl Pts',(64.3578269537903,-4.62303266683173,331.304011614975));
#15691=CARTESIAN_POINT('Ctrl Pts',(64.3504295045863,-4.71988931268382,331.428526359106));
#15692=CARTESIAN_POINT('Ctrl Pts',(64.3430320553823,-4.81162530113623,331.556717768761));
#15693=CARTESIAN_POINT('Ctrl Pts',(64.3356349269188,-4.90335731207604,331.68490362026));
#15694=CARTESIAN_POINT('Ctrl Pts',(64.3282377984553,-4.98996888987844,331.816765516812));
#15695=CARTESIAN_POINT('Ctrl Pts',(64.3208406699918,-5.07116500951098,331.951850395927));
#15696=CARTESIAN_POINT('Ctrl Pts',(64.3134424025552,-5.15237363131895,332.08695607474));
#15697=CARTESIAN_POINT('Ctrl Pts',(64.3060441351186,-5.22816494238112,332.225285404338));
#15698=CARTESIAN_POINT('Ctrl Pts',(64.298645867682,-5.29828901447146,332.366359158573));
#15699=CARTESIAN_POINT('Ctrl Pts',(64.2912450011562,-5.36843772188596,332.507482473502));
#15700=CARTESIAN_POINT('Ctrl Pts',(64.2838441346305,-5.43291506031164,332.651351798689));
#15701=CARTESIAN_POINT('Ctrl Pts',(64.2764432681047,-5.4915185960913,332.797466442643));
#15702=CARTESIAN_POINT('Ctrl Pts',(64.2690342747199,-5.55018648415592,332.943741534445));
#15703=CARTESIAN_POINT('Ctrl Pts',(64.2616252813351,-5.60296754957407,333.092266522304));
#15704=CARTESIAN_POINT('Ctrl Pts',(64.2542162879504,-5.6497085111847,333.242523314195));
#15705=CARTESIAN_POINT('Ctrl Pts',(64.2468027303701,-5.69647826683992,333.392872669453));
#15706=CARTESIAN_POINT('Ctrl Pts',(64.2393891727899,-5.73720040797205,333.544955594916));
#15707=CARTESIAN_POINT('Ctrl Pts',(64.2319756152096,-5.77177256728104,333.698242728431));
#15708=CARTESIAN_POINT('Ctrl Pts',(64.2245515030729,-5.80639394638803,333.851748094244));
#15709=CARTESIAN_POINT('Ctrl Pts',(64.2171273909362,-5.83484778961272,334.006460726064));
#15710=CARTESIAN_POINT('Ctrl Pts',(64.2097032787995,-5.85708335865905,334.16184423153));
#15711=CARTESIAN_POINT('Ctrl Pts',(64.205846153645,-5.86863563199691,334.24257221846));
#15712=CARTESIAN_POINT('Ctrl Pts',(64.2019890284904,-5.87851031382604,334.323481245407));
#15713=CARTESIAN_POINT('Ctrl Pts',(64.1981319033359,-5.88670584130011,334.404496095308));
#15714=CARTESIAN_POINT('Ctrl Pts',(64.1887719371252,-5.90659367411937,334.601092323655));
#15715=CARTESIAN_POINT('Ctrl Pts',(64.1794119709144,-5.91663528152812,334.798701233181));
#15716=CARTESIAN_POINT('Ctrl Pts',(64.1700520047036,-5.91674902275044,334.996599370386));
#15717=CARTESIAN_POINT('',(62.4200520047037,-5.90885860505928,334.996668088724));
#15718=CARTESIAN_POINT('Ctrl Pts',(64.1700494855937,-5.9240457458271,334.996648503969));
#15719=CARTESIAN_POINT('Ctrl Pts',(64.0866642800831,-5.91193315107515,336.761847268243));
#15720=CARTESIAN_POINT('Ctrl Pts',(63.9105330631479,-4.13709079260203,340.511496579727));
#15721=CARTESIAN_POINT('Ctrl Pts',(63.6416558347881,2.24304846138158,341.627318954231));
#15722=CARTESIAN_POINT('Ctrl Pts',(63.3634178005139,6.7868961248111,336.700195257098));
#15723=CARTESIAN_POINT('Ctrl Pts',(63.0851797662404,5.10250938892159,330.212827467371));
#15724=CARTESIAN_POINT('Ctrl Pts',(62.8069417319662,-1.26437490026262,328.118577252282));
#15725=CARTESIAN_POINT('Ctrl Pts',(62.5852324781208,-5.41315464388666,331.481794192749));
#15726=CARTESIAN_POINT('Ctrl Pts',(62.4562692356999,-5.91279898515629,334.22492707629));
#15727=CARTESIAN_POINT('Ctrl Pts',(62.4200520047037,-5.90885860505928,334.996668088724));
#15728=CARTESIAN_POINT('',(60.6700520047037,-5.91184663644443,335.00482244531));
#15729=CARTESIAN_POINT('Ctrl Pts',(62.4200520047037,-5.90885860505928,334.996668088724));
#15730=CARTESIAN_POINT('Ctrl Pts',(62.3635232242752,-5.90270835902497,336.201221198928));
#15731=CARTESIAN_POINT('Ctrl Pts',(62.2142484324222,-4.95843404406749,339.390925102401));
#15732=CARTESIAN_POINT('Ctrl Pts',(61.9722276291445,0.259294994690306,341.991808709264));
#15733=CARTESIAN_POINT('Ctrl Pts',(61.6939895948703,6.0198805072899,338.56562218963));
#15734=CARTESIAN_POINT('Ctrl Pts',(61.4157515605967,6.25611053163765,331.867316815072));
#15735=CARTESIAN_POINT('Ctrl Pts',(61.1375135263227,0.751200261145621,328.043828560992));
#15736=CARTESIAN_POINT('Ctrl Pts',(60.8889470076916,-4.78251313240014,330.330906474057));
#15737=CARTESIAN_POINT('Ctrl Pts',(60.7331265004854,-5.90158848196943,333.662495110449));
#15738=CARTESIAN_POINT('Ctrl Pts',(60.6700520047037,-5.91184663644443,335.00482244531));
#15739=CARTESIAN_POINT('',(58.9200526404505,-5.92193719492645,335.001095068209));
#15740=CARTESIAN_POINT('Ctrl Pts',(60.6700520047037,-5.91184663644443,335.00482244531));
#15741=CARTESIAN_POINT('Ctrl Pts',(60.6403804890607,-5.91667227931642,335.636280311452));
#15742=CARTESIAN_POINT('Ctrl Pts',(60.5179629619931,-5.53236301513891,338.23580376784));
#15743=CARTESIAN_POINT('Ctrl Pts',(60.3027994235009,-1.74600677399053,341.775255217807));
#15744=CARTESIAN_POINT('Ctrl Pts',(60.0245613892267,4.75259220513214,340.134733708085));
#15745=CARTESIAN_POINT('Ctrl Pts',(59.7463233549531,6.8898074657468,333.782142863004));
#15746=CARTESIAN_POINT('Ctrl Pts',(59.4680853206789,2.70434810844245,328.547161536998));
#15747=CARTESIAN_POINT('Ctrl Pts',(59.1926619252332,-3.89540661009425,329.226908277723));
#15748=CARTESIAN_POINT('Ctrl Pts',(59.0099845412119,-5.92134586278168,333.099183268187));
#15749=CARTESIAN_POINT('Ctrl Pts',(58.9200531686153,-5.92624669111755,335.001084705077));
#15750=CARTESIAN_POINT('',(57.1700520097339,-5.91552009762918,334.994582380634));
#15751=CARTESIAN_POINT('Ctrl Pts',(58.9200520047036,-5.91674989634092,335.001107542211));
#15752=CARTESIAN_POINT('Ctrl Pts',(58.9172377538462,-5.9167387733927,335.060528936766));
#15753=CARTESIAN_POINT('Ctrl Pts',(58.9144235029886,-5.91583252987226,335.11994095873));
#15754=CARTESIAN_POINT('Ctrl Pts',(58.9116092521311,-5.91403186056312,335.179325722484));
#15755=CARTESIAN_POINT('Ctrl Pts',(58.9041852746931,-5.90928170537042,335.335982384803));
#15756=CARTESIAN_POINT('Ctrl Pts',(58.8967612972551,-5.89829557337556,335.492686500929));
#15757=CARTESIAN_POINT('Ctrl Pts',(58.8893373198171,-5.88105925025173,335.64890111537));
#15758=CARTESIAN_POINT('Ctrl Pts',(58.8819221037895,-5.86384326858252,335.804931373062));
#15759=CARTESIAN_POINT('Ctrl Pts',(58.8745068877619,-5.84039181869279,335.960472911608));
#15760=CARTESIAN_POINT('Ctrl Pts',(58.8670916717343,-5.81074267411211,336.114988850954));
#15761=CARTESIAN_POINT('Ctrl Pts',(58.8596835905902,-5.78112205778905,336.269356115842));
#15762=CARTESIAN_POINT('Ctrl Pts',(58.8522755094461,-5.74531568863431,336.422699382042));
#15763=CARTESIAN_POINT('Ctrl Pts',(58.844867428302,-5.70341310147181,336.57448707726));
#15764=CARTESIAN_POINT('Ctrl Pts',(58.8374648611281,-5.66154170317029,336.726161794124));
#15765=CARTESIAN_POINT('Ctrl Pts',(58.8300622939541,-5.61358322062559,336.876282887221));
#15766=CARTESIAN_POINT('Ctrl Pts',(58.8226597267801,-5.55967818781155,337.024329274222));
#15767=CARTESIAN_POINT('Ctrl Pts',(58.8152610570254,-5.50580153576148,337.172297715448));
#15768=CARTESIAN_POINT('Ctrl Pts',(58.8078623872706,-5.44598469604835,337.318193276202));
#15769=CARTESIAN_POINT('Ctrl Pts',(58.8004637175159,-5.38041791224381,337.461510441194));
#15770=CARTESIAN_POINT('Ctrl Pts',(58.7930662683119,-5.31486194492279,337.604803963303));
#15771=CARTESIAN_POINT('Ctrl Pts',(58.7856688191079,-5.24355807121388,337.745519594793));
#15772=CARTESIAN_POINT('Ctrl Pts',(58.7782713699039,-5.16674454722182,337.883172097925));
#15773=CARTESIAN_POINT('Ctrl Pts',(58.7708742414405,-5.08993435373031,338.020818632684));
#15774=CARTESIAN_POINT('Ctrl Pts',(58.763477112977,-5.00761516680744,338.155401977256));
#15775=CARTESIAN_POINT('Ctrl Pts',(58.7560799845136,-4.92007091887895,338.286462036248));
#15776=CARTESIAN_POINT('Ctrl Pts',(58.748681717077,-4.83251319132162,338.417542275219));
#15777=CARTESIAN_POINT('Ctrl Pts',(58.7412834496404,-4.73972900814861,338.545097838062));
#15778=CARTESIAN_POINT('Ctrl Pts',(58.7338851822038,-4.64204520212892,338.668698257406));
#15779=CARTESIAN_POINT('Ctrl Pts',(58.7264843156781,-4.54432707876063,338.792342098876));
#15780=CARTESIAN_POINT('Ctrl Pts',(58.7190834491523,-4.44170613672706,338.912027737765));
#15781=CARTESIAN_POINT('Ctrl Pts',(58.7116825826266,-4.33454888248113,339.027358507494));
#15782=CARTESIAN_POINT('Ctrl Pts',(58.7042735892418,-4.22727395932564,339.142815921433));
#15783=CARTESIAN_POINT('Ctrl Pts',(58.6968645958571,-4.11545303021221,339.253908642604));
#15784=CARTESIAN_POINT('Ctrl Pts',(58.6894556024723,-3.99948930601635,339.360277038625));
#15785=CARTESIAN_POINT('Ctrl Pts',(58.6820420448921,-3.88345414416653,339.466710961247));
#15786=CARTESIAN_POINT('Ctrl Pts',(58.6746284873118,-3.76327138605488,339.568414518944));
#15787=CARTESIAN_POINT('Ctrl Pts',(58.6672149297316,-3.63937615359108,339.665069321583));
#15788=CARTESIAN_POINT('Ctrl Pts',(58.659790817595,-3.51530453358173,339.761861730028));
#15789=CARTESIAN_POINT('Ctrl Pts',(58.6523667054583,-3.38751018561926,339.853590810846));
#15790=CARTESIAN_POINT('Ctrl Pts',(58.6449425933216,-3.25645661285392,339.939981871536));
#15791=CARTESIAN_POINT('Ctrl Pts',(58.6410854681668,-3.18836900549629,339.984865505727));
#15792=CARTESIAN_POINT('Ctrl Pts',(58.637228343012,-3.11940206680971,340.028309047847));
#15793=CARTESIAN_POINT('Ctrl Pts',(58.6333712178572,-3.04962316104359,340.070279000028));
#15794=CARTESIAN_POINT('Ctrl Pts',(58.6259472404192,-2.91531665003766,340.151060402125));
#15795=CARTESIAN_POINT('Ctrl Pts',(58.6185232629812,-2.77759558924419,340.226623518268));
#15796=CARTESIAN_POINT('Ctrl Pts',(58.6110992855432,-2.63690382380578,340.296665817899));
#15797=CARTESIAN_POINT('Ctrl Pts',(58.6036840695155,-2.4963780958186,340.366625457078));
#15798=CARTESIAN_POINT('Ctrl Pts',(58.5962688534879,-2.35288897254252,340.43107708403));
#15799=CARTESIAN_POINT('Ctrl Pts',(58.5888536374603,-2.2069083692926,340.489761926718));
#15800=CARTESIAN_POINT('Ctrl Pts',(58.5814455563162,-2.06106822784422,340.548390303147));
#15801=CARTESIAN_POINT('Ctrl Pts',(58.5740374751721,-1.91274172294228,340.601262803605));
#15802=CARTESIAN_POINT('Ctrl Pts',(58.566629394028,-1.76242431750096,340.648167055566));
#15803=CARTESIAN_POINT('Ctrl Pts',(58.559226826854,-1.61221879604985,340.695036395836));
#15804=CARTESIAN_POINT('Ctrl Pts',(58.55182425968,-1.46002567940949,340.735946222136));
#15805=CARTESIAN_POINT('Ctrl Pts',(58.5444216925059,-1.30635920782263,340.770732724935));
#15806=CARTESIAN_POINT('Ctrl Pts',(58.5370230227512,-1.15277364096126,340.805500912793));
#15807=CARTESIAN_POINT('Ctrl Pts',(58.5296243529965,-0.997716627119905,
340.834152115551));
#15808=CARTESIAN_POINT('Ctrl Pts',(58.5222256832417,-0.841716216602509,
340.856572749758));
#15809=CARTESIAN_POINT('Ctrl Pts',(58.5148282340377,-0.685741541308998,
340.878989685257));
#15810=CARTESIAN_POINT('Ctrl Pts',(58.5074307848337,-0.528824147273298,
340.895178039114));
#15811=CARTESIAN_POINT('Ctrl Pts',(58.5000333356298,-0.371501015311117,
340.905075575987));
#15812=CARTESIAN_POINT('Ctrl Pts',(58.4926362071663,-0.214184704605776,
340.914972683721));
#15813=CARTESIAN_POINT('Ctrl Pts',(58.4852390787028,-0.0564630634277288,
340.918579493373));
#15814=CARTESIAN_POINT('Ctrl Pts',(58.4778419502394,0.101123352065179,340.915885785761));
#15815=CARTESIAN_POINT('Ctrl Pts',(58.4704436828028,0.258734031932412,340.913191663385));
#15816=CARTESIAN_POINT('Ctrl Pts',(58.4630454153662,0.416209071476924,340.904195098482));
#15817=CARTESIAN_POINT('Ctrl Pts',(58.4556471479296,0.573009613535163,340.888937981105));
#15818=CARTESIAN_POINT('Ctrl Pts',(58.4482462814038,0.729865241272778,340.873675503741));
#15819=CARTESIAN_POINT('Ctrl Pts',(58.4408454148781,0.886045528518061,340.852148131026));
#15820=CARTESIAN_POINT('Ctrl Pts',(58.4334445483523,1.04101857221098,340.824449407009));
#15821=CARTESIAN_POINT('Ctrl Pts',(58.4260355549675,1.19616179112189,340.796720267145));
#15822=CARTESIAN_POINT('Ctrl Pts',(58.4186265615828,1.35009475144059,340.762806308183));
#15823=CARTESIAN_POINT('Ctrl Pts',(58.411217568198,1.50229683008476,340.722851981033));
#15824=CARTESIAN_POINT('Ctrl Pts',(58.4038040106178,1.65459267045927,340.68287304064));
#15825=CARTESIAN_POINT('Ctrl Pts',(58.3963904530376,1.80515514837665,340.636846426176));
#15826=CARTESIAN_POINT('Ctrl Pts',(58.3889768954573,1.95348105334845,340.584965741767));
#15827=CARTESIAN_POINT('Ctrl Pts',(58.3815527833207,2.10201812740078,340.533011195706));
#15828=CARTESIAN_POINT('Ctrl Pts',(58.374128671184,2.24831192293559,340.475186071175));
#15829=CARTESIAN_POINT('Ctrl Pts',(58.3667045590473,2.39188061701794,340.411731485988));
#15830=CARTESIAN_POINT('Ctrl Pts',(58.3628474338926,2.46647033376405,340.37876427426));
#15831=CARTESIAN_POINT('Ctrl Pts',(58.3589903087379,2.54032490300279,340.344278297606));
#15832=CARTESIAN_POINT('Ctrl Pts',(58.3551331835833,2.61337970100166,340.308312076441));
#15833=CARTESIAN_POINT('Ctrl Pts',(58.3477092061453,2.75399146503163,340.239086317943));
#15834=CARTESIAN_POINT('Ctrl Pts',(58.3402852287073,2.89206286989311,340.164165277727));
#15835=CARTESIAN_POINT('Ctrl Pts',(58.3328612512693,3.02709932111036,340.083758478));
#15836=CARTESIAN_POINT('Ctrl Pts',(58.3254460352417,3.16197640899775,340.003446570393));
#15837=CARTESIAN_POINT('Ctrl Pts',(58.318030819214,3.2938253551254,339.917661979002));
#15838=CARTESIAN_POINT('Ctrl Pts',(58.3106156031864,3.42217317211194,339.826661511084));
#15839=CARTESIAN_POINT('Ctrl Pts',(58.3032075220423,3.55039749347531,339.735748603358));
#15840=CARTESIAN_POINT('Ctrl Pts',(58.2957994408982,3.67512708987139,339.6396300248));
#15841=CARTESIAN_POINT('Ctrl Pts',(58.2883913597541,3.79591524929912,339.538607493785));
#15842=CARTESIAN_POINT('Ctrl Pts',(58.2809887925801,3.91661350389376,339.437660155684));
#15843=CARTESIAN_POINT('Ctrl Pts',(58.2735862254061,4.03337587785536,339.33181637142));
#15844=CARTESIAN_POINT('Ctrl Pts',(58.2661836582321,4.14578633535286,339.221419929846));
#15845=CARTESIAN_POINT('Ctrl Pts',(58.2587849884773,4.25813760923585,339.111081611516));
#15846=CARTESIAN_POINT('Ctrl Pts',(58.2513863187226,4.36614126424074,338.996195670399));
#15847=CARTESIAN_POINT('Ctrl Pts',(58.2439876489678,4.46941602730123,338.877144688737));
#15848=CARTESIAN_POINT('Ctrl Pts',(58.2365901997639,4.57267375323266,338.758113346791));
#15849=CARTESIAN_POINT('Ctrl Pts',(58.2291927505599,4.67120389118536,338.63491860962));
#15850=CARTESIAN_POINT('Ctrl Pts',(58.2217953013559,4.76466351500142,338.507978356734));
#15851=CARTESIAN_POINT('Ctrl Pts',(58.2143981728924,4.85811908657106,338.381043607756));
#15852=CARTESIAN_POINT('Ctrl Pts',(58.207001044429,4.9465043598626,338.250363966507));
#15853=CARTESIAN_POINT('Ctrl Pts',(58.1996039159655,5.02951821539355,338.116388468007));
#15854=CARTESIAN_POINT('Ctrl Pts',(58.1922056485289,5.11254485298595,337.982392340624));
#15855=CARTESIAN_POINT('Ctrl Pts',(58.1848073810922,5.19019822943935,337.845099662797));
#15856=CARTESIAN_POINT('Ctrl Pts',(58.1774091136556,5.26222196446109,337.704986240121));
#15857=CARTESIAN_POINT('Ctrl Pts',(58.1700082471299,5.33427100217847,337.564823594126));
#15858=CARTESIAN_POINT('Ctrl Pts',(58.1626073806042,5.40068629024772,337.421838562005));
#15859=CARTESIAN_POINT('Ctrl Pts',(58.1552065140784,5.46125864858901,337.27652905444));
#15860=CARTESIAN_POINT('Ctrl Pts',(58.1477975206936,5.52189752117071,337.131059983145));
#15861=CARTESIAN_POINT('Ctrl Pts',(58.1403885273089,5.57668050705673,336.98326168362));
#15862=CARTESIAN_POINT('Ctrl Pts',(58.1329795339241,5.62544733907619,336.8336501296));
#15863=CARTESIAN_POINT('Ctrl Pts',(58.1255659763439,5.67424421314632,336.683946409701));
#15864=CARTESIAN_POINT('Ctrl Pts',(58.1181524187636,5.71701744718284,336.532427567818));
#15865=CARTESIAN_POINT('Ctrl Pts',(58.1107388611834,5.75365753095644,336.379621534686));
#15866=CARTESIAN_POINT('Ctrl Pts',(58.1033147490467,5.79034977859712,336.226597954191));
#15867=CARTESIAN_POINT('Ctrl Pts',(58.09589063691,5.82089136483445,336.072283887596));
#15868=CARTESIAN_POINT('Ctrl Pts',(58.0884665247733,5.84522430874448,335.91721499277));
#15869=CARTESIAN_POINT('Ctrl Pts',(58.0846093996187,5.85786625276605,335.836650458733));
#15870=CARTESIAN_POINT('Ctrl Pts',(58.080752274464,5.86883320446076,335.75588223507));
#15871=CARTESIAN_POINT('Ctrl Pts',(58.0768951493094,5.87812258485851,335.674985510864));
#15872=CARTESIAN_POINT('Ctrl Pts',(58.0694711718714,5.89600226148839,335.519280048574));
#15873=CARTESIAN_POINT('Ctrl Pts',(58.0620471944334,5.90771792010705,335.362628784773));
#15874=CARTESIAN_POINT('Ctrl Pts',(58.0546232169954,5.91317809895577,335.205561018994));
#15875=CARTESIAN_POINT('Ctrl Pts',(58.0472080009677,5.91863183397192,335.048678616811));
#15876=CARTESIAN_POINT('Ctrl Pts',(58.0397927849401,5.9178447711773,334.891381060417));
#15877=CARTESIAN_POINT('Ctrl Pts',(58.0323775689125,5.91077690466284,334.734205068136));
#15878=CARTESIAN_POINT('Ctrl Pts',(58.0249694877684,5.90371583881395,334.577180309804));
#15879=CARTESIAN_POINT('Ctrl Pts',(58.0175614066243,5.89038601709737,334.420277253065));
#15880=CARTESIAN_POINT('Ctrl Pts',(58.0101533254802,5.87079941943505,334.264034824695));
#15881=CARTESIAN_POINT('Ctrl Pts',(58.0027507583062,5.85122740043508,334.107908690419));
#15882=CARTESIAN_POINT('Ctrl Pts',(57.9953481911322,5.82540792454322,333.952442574158));
#15883=CARTESIAN_POINT('Ctrl Pts',(57.9879456239582,5.7934049502816,333.798172373195));
#15884=CARTESIAN_POINT('Ctrl Pts',(57.9805469542034,5.76141882544605,333.643983394817));
#15885=CARTESIAN_POINT('Ctrl Pts',(57.9731482844486,5.72325576154802,333.490989442274));
#15886=CARTESIAN_POINT('Ctrl Pts',(57.9657496146939,5.67903115142419,333.339718173425));
#15887=CARTESIAN_POINT('Ctrl Pts',(57.9583521654899,5.63481383698776,333.188471859639));
#15888=CARTESIAN_POINT('Ctrl Pts',(57.9509547162859,5.58453706556066,333.03894802339));
#15889=CARTESIAN_POINT('Ctrl Pts',(57.943557267082,5.52836666391632,332.891661177183));
#15890=CARTESIAN_POINT('Ctrl Pts',(57.9361601386185,5.47219869772271,332.744380717076));
#15891=CARTESIAN_POINT('Ctrl Pts',(57.928763010155,5.41013774239253,332.599337402872));
#15892=CARTESIAN_POINT('Ctrl Pts',(57.9213658816916,5.3423984480232,332.457027450982));
#15893=CARTESIAN_POINT('Ctrl Pts',(57.913967614255,5.27464872349348,332.314695586912));
#15894=CARTESIAN_POINT('Ctrl Pts',(57.9065693468184,5.20121907944653,332.175098260165));
#15895=CARTESIAN_POINT('Ctrl Pts',(57.8991710793817,5.12237088887098,332.03870855211));
#15896=CARTESIAN_POINT('Ctrl Pts',(57.891770212856,5.04349499809679,331.902270928916));
#15897=CARTESIAN_POINT('Ctrl Pts',(57.8843693463302,4.95919695741673,331.76904349091));
#15898=CARTESIAN_POINT('Ctrl Pts',(57.8769684798044,4.86978227120296,331.639471590125));
#15899=CARTESIAN_POINT('Ctrl Pts',(57.8695594864197,4.7802693991154,331.509757407006));
#15900=CARTESIAN_POINT('Ctrl Pts',(57.8621504930349,4.68562887301656,331.383707084893));
#15901=CARTESIAN_POINT('Ctrl Pts',(57.8547414996501,4.58620785646418,331.261734618863));
#15902=CARTESIAN_POINT('Ctrl Pts',(57.8473279420699,4.48672559313621,331.139687013587));
#15903=CARTESIAN_POINT('Ctrl Pts',(57.8399143844896,4.38245721774821,331.021722549066));
#15904=CARTESIAN_POINT('Ctrl Pts',(57.8325008269094,4.27378741625107,330.908219008403));
#15905=CARTESIAN_POINT('Ctrl Pts',(57.8250767147727,4.16496290339691,330.79455387467));
#15906=CARTESIAN_POINT('Ctrl Pts',(57.817652602636,4.05172471743978,330.685362607253));
#15907=CARTESIAN_POINT('Ctrl Pts',(57.8102284904993,3.93449192770485,330.580983838757));
#15908=CARTESIAN_POINT('Ctrl Pts',(57.8063713653446,3.87358477356824,330.526754866166));
#15909=CARTESIAN_POINT('Ctrl Pts',(57.80251424019,3.81159989802079,330.473824202212));
#15910=CARTESIAN_POINT('Ctrl Pts',(57.7986571150353,3.74859913353756,330.422234704734));
#15911=CARTESIAN_POINT('Ctrl Pts',(57.7912331375973,3.62733880742767,330.322938143187));
#15912=CARTESIAN_POINT('Ctrl Pts',(57.7838091601593,3.50194743281196,330.228313208422));
#15913=CARTESIAN_POINT('Ctrl Pts',(57.7763851827213,3.37282061375475,330.138723246931));
#15914=CARTESIAN_POINT('Ctrl Pts',(57.7689699666937,3.2438461837722,330.049239015074));
#15915=CARTESIAN_POINT('Ctrl Pts',(57.7615547506661,3.11114538796478,329.964778139473));
#15916=CARTESIAN_POINT('Ctrl Pts',(57.7541395346385,2.97514791472798,329.885664711031));
#15917=CARTESIAN_POINT('Ctrl Pts',(57.7467314534944,2.83928129757518,329.806627405133));
#15918=CARTESIAN_POINT('Ctrl Pts',(57.7393233723502,2.70012463838737,329.732927489496));
#15919=CARTESIAN_POINT('Ctrl Pts',(57.7319152912061,2.55813761521197,329.664846534153));
#15920=CARTESIAN_POINT('Ctrl Pts',(57.7245127240321,2.41625627557101,329.596816252708));
#15921=CARTESIAN_POINT('Ctrl Pts',(57.7171101568582,2.27154910175669,329.534396764668));
#15922=CARTESIAN_POINT('Ctrl Pts',(57.7097075896842,2.12450135285257,329.477824290714));
#15923=CARTESIAN_POINT('Ctrl Pts',(57.7023089199294,1.9775310239458,329.421281601921));
#15924=CARTESIAN_POINT('Ctrl Pts',(57.6949102501746,1.82822292159833,329.370579930014));
#15925=CARTESIAN_POINT('Ctrl Pts',(57.6875115804199,1.6770832102468,329.32590778464));
#15926=CARTESIAN_POINT('Ctrl Pts',(57.6801141312159,1.5259684322543,329.281243008783));
#15927=CARTESIAN_POINT('Ctrl Pts',(57.672716682012,1.3730230025021,329.242605891014));
#15928=CARTESIAN_POINT('Ctrl Pts',(57.665319232808,1.21876932391259,329.210135416299));
#15929=CARTESIAN_POINT('Ctrl Pts',(57.6579221043445,1.06452233349377,329.177666349448));
#15930=CARTESIAN_POINT('Ctrl Pts',(57.650524975881,0.908967572230166,329.151363470898));
#15931=CARTESIAN_POINT('Ctrl Pts',(57.6431278474176,0.752638478572933,329.131314807977));
#15932=CARTESIAN_POINT('Ctrl Pts',(57.635729579981,0.596285314137554,329.111263058062));
#15933=CARTESIAN_POINT('Ctrl Pts',(57.6283313125444,0.439157950112207,329.097467488698));
#15934=CARTESIAN_POINT('Ctrl Pts',(57.6209330451077,0.281795654633014,329.089964317237));
#15935=CARTESIAN_POINT('Ctrl Pts',(57.613532178582,0.124378076124673,329.082458509833));
#15936=CARTESIAN_POINT('Ctrl Pts',(57.6061313120562,-0.0332742256094407,
329.081249519367));
#15937=CARTESIAN_POINT('Ctrl Pts',(57.5987304455305,-0.190621418598294,
329.086321446234));
#15938=CARTESIAN_POINT('Ctrl Pts',(57.5913214521457,-0.348141393848144,
329.091398942562));
#15939=CARTESIAN_POINT('Ctrl Pts',(57.5839124587609,-0.505355218022771,
329.102771117964));
#15940=CARTESIAN_POINT('Ctrl Pts',(57.5765034653762,-0.661726883708614,
329.12037007169));
#15941=CARTESIAN_POINT('Ctrl Pts',(57.5690899077959,-0.818194879734465,
329.137979866979));
#15942=CARTESIAN_POINT('Ctrl Pts',(57.5616763502157,-0.973819315452161,
329.161824027759));
#15943=CARTESIAN_POINT('Ctrl Pts',(57.5542627926354,-1.12807432934979,329.191783503522));
#15944=CARTESIAN_POINT('Ctrl Pts',(57.5468386804987,-1.28254895349975,329.221785632083));
#15945=CARTESIAN_POINT('Ctrl Pts',(57.539414568362,-1.43564989979138,329.257920378292));
#15946=CARTESIAN_POINT('Ctrl Pts',(57.5319904562253,-1.58686562238468,329.300018591347));
#15947=CARTESIAN_POINT('Ctrl Pts',(57.5281333310707,-1.66542827831582,329.32189030793));
#15948=CARTESIAN_POINT('Ctrl Pts',(57.5242762059161,-1.74348237571021,329.345370892741));
#15949=CARTESIAN_POINT('Ctrl Pts',(57.5204190807615,-1.8209584133973,329.370431542367));
#15950=CARTESIAN_POINT('Ctrl Pts',(57.5129951033235,-1.97007993077494,329.41866687048));
#15951=CARTESIAN_POINT('Ctrl Pts',(57.5055711258855,-2.11750852491339,329.472904170722));
#15952=CARTESIAN_POINT('Ctrl Pts',(57.4981471484475,-2.26272456593604,329.533007398833));
#15953=CARTESIAN_POINT('Ctrl Pts',(57.4907319324199,-2.40776923018144,329.593039696092));
#15954=CARTESIAN_POINT('Ctrl Pts',(57.4833167163922,-2.55060619734944,329.658924000182));
#15955=CARTESIAN_POINT('Ctrl Pts',(57.4759015003646,-2.69073040343831,329.730474361149));
#15956=CARTESIAN_POINT('Ctrl Pts',(57.4684934192206,-2.83071978272151,329.801955876718));
#15957=CARTESIAN_POINT('Ctrl Pts',(57.4610853380765,-2.96800126719247,329.879092426955));
#15958=CARTESIAN_POINT('Ctrl Pts',(57.4536772569324,-3.10208932043758,329.961649832482));
#15959=CARTESIAN_POINT('Ctrl Pts',(57.4462746897584,-3.23607756949592,330.044145789025));
#15960=CARTESIAN_POINT('Ctrl Pts',(57.4388721225844,-3.36687680369746,330.132054372069));
#15961=CARTESIAN_POINT('Ctrl Pts',(57.4314695554104,-3.49402577849576,330.225095349464));
#15962=CARTESIAN_POINT('Ctrl Pts',(57.4240708856557,-3.6211078099147,330.318087341192));
#15963=CARTESIAN_POINT('Ctrl Pts',(57.4166722159009,-3.74454310897152,330.416206125874));
#15964=CARTESIAN_POINT('Ctrl Pts',(57.4092735461462,-3.86389923926214,330.519128072425));
#15965=CARTESIAN_POINT('Ctrl Pts',(57.4018760969422,-3.9832356794973,330.62203304005));
#15966=CARTESIAN_POINT('Ctrl Pts',(57.3944786477382,-4.09849400416171,330.729739353454));
#15967=CARTESIAN_POINT('Ctrl Pts',(57.3870811985343,-4.20927463563525,330.841882925614));
#15968=CARTESIAN_POINT('Ctrl Pts',(57.3796840700708,-4.32005046385366,330.954021635424));
#15969=CARTESIAN_POINT('Ctrl Pts',(57.3722869416074,-4.4263487226235,331.070596955944));
#15970=CARTESIAN_POINT('Ctrl Pts',(57.3648898131439,-4.52780671373297,331.191207944036));
#15971=CARTESIAN_POINT('Ctrl Pts',(57.3574915457073,-4.62928032684041,331.31183750321));
#15972=CARTESIAN_POINT('Ctrl Pts',(57.3500932782707,-4.72591194807402,331.436503681611));
#15973=CARTESIAN_POINT('Ctrl Pts',(57.3426950108341,-4.81737929255915,331.564772596447));
#15974=CARTESIAN_POINT('Ctrl Pts',(57.3352941443084,-4.90887877048416,331.693086573501));
#15975=CARTESIAN_POINT('Ctrl Pts',(57.3278932777826,-4.99521014291513,331.82500550328));
#15976=CARTESIAN_POINT('Ctrl Pts',(57.3204924112569,-5.07609464611404,331.960066825374));
#15977=CARTESIAN_POINT('Ctrl Pts',(57.3130834178722,-5.15706796823044,332.095276457712));
#15978=CARTESIAN_POINT('Ctrl Pts',(57.3056744244875,-5.2325822845081,332.233635053115));
#15979=CARTESIAN_POINT('Ctrl Pts',(57.2982654311027,-5.30240462976961,332.374655126522));
#15980=CARTESIAN_POINT('Ctrl Pts',(57.2908518735225,-5.37226998800428,332.515762073158));
#15981=CARTESIAN_POINT('Ctrl Pts',(57.2834383159423,-5.43643623640651,332.65953342483));
#15982=CARTESIAN_POINT('Ctrl Pts',(57.2760247583621,-5.49471891325114,332.805462548312));
#15983=CARTESIAN_POINT('Ctrl Pts',(57.2686006462254,-5.55308456615629,332.951599428617));
#15984=CARTESIAN_POINT('Ctrl Pts',(57.2611765340887,-5.605549794137,333.099899865204));
#15985=CARTESIAN_POINT('Ctrl Pts',(57.2537524219521,-5.65198001290537,333.249842151057));
#15986=CARTESIAN_POINT('Ctrl Pts',(57.2498952967972,-5.67610238086791,333.327743205336));
#15987=CARTESIAN_POINT('Ctrl Pts',(57.2460381716424,-5.69859660700881,333.406087252807));
#15988=CARTESIAN_POINT('Ctrl Pts',(57.2421810464875,-5.71944930166043,333.484800261274));
#15989=CARTESIAN_POINT('Ctrl Pts',(57.2326002064978,-5.77124599551726,333.680318090994));
#15990=CARTESIAN_POINT('Ctrl Pts',(57.2230193665081,-5.81303845332948,333.878589080625));
#15991=CARTESIAN_POINT('Ctrl Pts',(57.2134385265183,-5.8445851370561,334.078720922737));
#15992=CARTESIAN_POINT('Ctrl Pts',(57.2040376317612,-5.87553931789689,334.275093932541));
#15993=CARTESIAN_POINT('Ctrl Pts',(57.1946367370041,-5.89662901993686,334.473258743316));
#15994=CARTESIAN_POINT('Ctrl Pts',(57.185235842247,-5.90767099538767,334.672350838922));
#15995=CARTESIAN_POINT('Ctrl Pts',(57.1801745706339,-5.91361579514823,334.779538420307));
#15996=CARTESIAN_POINT('Ctrl Pts',(57.1751132990208,-5.91664898040585,334.88699439044));
#15997=CARTESIAN_POINT('Ctrl Pts',(57.1700520274078,-5.9167475183286,334.994580880855));
#15998=CARTESIAN_POINT('',(55.4200520047037,-5.9073516651236,335.001572401572));
#15999=CARTESIAN_POINT('Ctrl Pts',(57.1700520047036,-5.91517075142323,334.994582807498));
#16000=CARTESIAN_POINT('Ctrl Pts',(57.1013490072069,-5.90207856338616,336.454613423218));
#16001=CARTESIAN_POINT('Ctrl Pts',(56.9398999982855,-4.61904585079844,339.906179566562));
#16002=CARTESIAN_POINT('Ctrl Pts',(56.6857049779395,1.1712837905338,341.897877731828));
#16003=CARTESIAN_POINT('Ctrl Pts',(56.4074669436658,6.43442141176684,337.747879913133));
#16004=CARTESIAN_POINT('Ctrl Pts',(56.1292289093918,5.7927854753311,331.076193256795));
#16005=CARTESIAN_POINT('Ctrl Pts',(55.8509908751177,-0.164804190445459,
328.005326133404));
#16006=CARTESIAN_POINT('Ctrl Pts',(55.6145985735551,-5.09790670228151,330.849837736591));
#16007=CARTESIAN_POINT('Ctrl Pts',(55.4709522834171,-5.90477649463899,333.916263515696));
#16008=CARTESIAN_POINT('Ctrl Pts',(55.4200520047037,-5.9073516651236,335.001572401572));
#16009=CARTESIAN_POINT('',(53.6700520047037,-5.92095424708517,335.00477685681));
#16010=CARTESIAN_POINT('Ctrl Pts',(55.4200520047037,-5.9073516651236,335.001572401572));
#16011=CARTESIAN_POINT('Ctrl Pts',(55.3782062719925,-5.90946874382158,335.893817919584));
#16012=CARTESIAN_POINT('Ctrl Pts',(55.2436145278565,-5.30035127753471,338.760873686747));
#16013=CARTESIAN_POINT('Ctrl Pts',(55.0162767722962,-0.845117328821545,
341.945386931031));
#16014=CARTESIAN_POINT('Ctrl Pts',(54.7380387380219,5.38318256419084,339.469224586192));
#16015=CARTESIAN_POINT('Ctrl Pts',(54.4598007037483,6.67141527368653,332.891720804254));
#16016=CARTESIAN_POINT('Ctrl Pts',(54.1815626694741,1.83738865645259,328.248953722098));
#16017=CARTESIAN_POINT('Ctrl Pts',(53.9183131031261,-4.33154583340499,329.717886501529));
#16018=CARTESIAN_POINT('Ctrl Pts',(53.7478095482025,-5.90649086568565,333.356466118773));
#16019=CARTESIAN_POINT('Ctrl Pts',(53.6700520047037,-5.92095424708517,335.00477685681));
#16020=CARTESIAN_POINT('',(51.9200520047037,-5.92019556150583,334.995902038103));
#16021=CARTESIAN_POINT('Ctrl Pts',(53.6700520047037,-5.92095424708517,335.00477685681));
#16022=CARTESIAN_POINT('Ctrl Pts',(53.6550635367779,-5.92374219431769,335.322503620248));
#16023=CARTESIAN_POINT('Ctrl Pts',(53.5473290574271,-5.75582090692233,337.603316580136));
#16024=CARTESIAN_POINT('Ctrl Pts',(53.3468485666526,-2.79128630412854,341.41571069248));
#16025=CARTESIAN_POINT('Ctrl Pts',(53.0686105323781,3.88458281135488,340.819161391726));
#16026=CARTESIAN_POINT('Ctrl Pts',(52.7903724981046,6.99562761720305,334.882453572468));
#16027=CARTESIAN_POINT('Ctrl Pts',(52.5121344638305,3.6868882140429,329.053616374772));
#16028=CARTESIAN_POINT('Ctrl Pts',(52.2338964295567,-3.00525408476659,328.681687661471));
#16029=CARTESIAN_POINT('Ctrl Pts',(52.0365356098476,-5.79592130595738,332.530685836328));
#16030=CARTESIAN_POINT('Ctrl Pts',(51.9319208015634,-5.92475043617385,334.744504705933));
#16031=CARTESIAN_POINT('Ctrl Pts',(51.9200520047037,-5.92276479782944,334.995900259677));
#16032=CARTESIAN_POINT('',(50.1700520295874,-5.91196191274669,334.997409895193));
#16033=CARTESIAN_POINT('Ctrl Pts',(51.9200520047037,-5.91674858252048,334.995904424104));
#16034=CARTESIAN_POINT('Ctrl Pts',(51.9127391591387,-5.91685569133361,335.150641128864));
#16035=CARTESIAN_POINT('Ctrl Pts',(51.9054263135738,-5.91088856752764,335.305614441861));
#16036=CARTESIAN_POINT('Ctrl Pts',(51.8981134680088,-5.89881806647569,335.460299881729));
#16037=CARTESIAN_POINT('Ctrl Pts',(51.8908080257001,-5.88675978515568,335.61482872374));
#16038=CARTESIAN_POINT('Ctrl Pts',(51.8835025833913,-5.86861045034028,335.769069892076));
#16039=CARTESIAN_POINT('Ctrl Pts',(51.8761971410826,-5.84439292948739,335.922497614229));
#16040=CARTESIAN_POINT('Ctrl Pts',(51.8688973956181,-5.82019429365704,336.075805692178));
#16041=CARTESIAN_POINT('Ctrl Pts',(51.8615976501536,-5.7899369485819,336.228301208236));
#16042=CARTESIAN_POINT('Ctrl Pts',(51.8542979046891,-5.75369566429892,336.379462491381));
#16043=CARTESIAN_POINT('Ctrl Pts',(51.8469280070357,-5.71710609315713,336.532076468312));
#16044=CARTESIAN_POINT('Ctrl Pts',(51.8395581093824,-5.67441698959474,336.683330036368));
#16045=CARTESIAN_POINT('Ctrl Pts',(51.832188211729,-5.62575849370094,336.832695264645));
#16046=CARTESIAN_POINT('Ctrl Pts',(51.8248937832169,-5.57759826997733,336.980530964828));
#16047=CARTESIAN_POINT('Ctrl Pts',(51.8175993547047,-5.5235904729516,337.126516449146));
#16048=CARTESIAN_POINT('Ctrl Pts',(51.8103049261926,-5.46391165425848,337.270154179116));
#16049=CARTESIAN_POINT('Ctrl Pts',(51.8030107439393,-5.40423485031395,337.413787059896));
#16050=CARTESIAN_POINT('Ctrl Pts',(51.7957165616861,-5.3388875529823,337.555071988646));
#16051=CARTESIAN_POINT('Ctrl Pts',(51.7884223794329,-5.26809454556195,337.693531217848));
#16052=CARTESIAN_POINT('Ctrl Pts',(51.7811269090558,-5.19728903637546,337.832014898404));
#16053=CARTESIAN_POINT('Ctrl Pts',(51.7738314386787,-5.12103607899454,337.967671544158));
#16054=CARTESIAN_POINT('Ctrl Pts',(51.7665359683016,-5.03960636180203,338.100048109398));
#16055=CARTESIAN_POINT('Ctrl Pts',(51.7591096676938,-4.95671635923634,338.234798593752));
#16056=CARTESIAN_POINT('Ctrl Pts',(51.7516833670861,-4.86846236842017,338.366149874553));
#16057=CARTESIAN_POINT('Ctrl Pts',(51.7442570664783,-4.77517532000896,338.493655853927));
#16058=CARTESIAN_POINT('Ctrl Pts',(51.7369507764448,-4.68339580985058,338.619101309952));
#16059=CARTESIAN_POINT('Ctrl Pts',(51.7296444864112,-4.58674497578895,338.740824547462));
#16060=CARTESIAN_POINT('Ctrl Pts',(51.7223381963777,-4.4855775118768,338.85843555699));
#16061=CARTESIAN_POINT('Ctrl Pts',(51.7148518904828,-4.38191743569982,338.978944322709));
#16062=CARTESIAN_POINT('Ctrl Pts',(51.707365584588,-4.27351558957195,339.095135287745));
#16063=CARTESIAN_POINT('Ctrl Pts',(51.6998792786932,-4.16079164584239,339.206630889725));
#16064=CARTESIAN_POINT('Ctrl Pts',(51.6923929727983,-4.04806770211283,339.318126491705));
#16065=CARTESIAN_POINT('Ctrl Pts',(51.6849066669035,-3.93102202258054,339.424926494386));
#16066=CARTESIAN_POINT('Ctrl Pts',(51.6774203610087,-3.81010768033821,339.526699683735));
#16067=CARTESIAN_POINT('Ctrl Pts',(51.6699963835707,-3.69020003011022,339.627625543851));
#16068=CARTESIAN_POINT('Ctrl Pts',(51.6625724061327,-3.56609858956593,339.723936018681));
#16069=CARTESIAN_POINT('Ctrl Pts',(51.6551484286947,-3.43819401744272,339.815262449848));
#16070=CARTESIAN_POINT('Ctrl Pts',(51.6477332126671,-3.31044039195871,339.906481102086));
#16071=CARTESIAN_POINT('Ctrl Pts',(51.6403179966395,-3.1788928696426,339.992727203956));
#16072=CARTESIAN_POINT('Ctrl Pts',(51.6329027806118,-3.04397672083853,340.073670888567));
#16073=CARTESIAN_POINT('Ctrl Pts',(51.6254946994677,-2.90919038767392,340.154536689572));
#16074=CARTESIAN_POINT('Ctrl Pts',(51.6180866183237,-2.77104219868998,340.230110039646));
#16075=CARTESIAN_POINT('Ctrl Pts',(51.6106785371796,-2.62998798564979,340.300103183697));
#16076=CARTESIAN_POINT('Ctrl Pts',(51.6032759700056,-2.48903876183643,340.370044230573));
#16077=CARTESIAN_POINT('Ctrl Pts',(51.5958734028316,-2.34518815371135,340.434413176366));
#16078=CARTESIAN_POINT('Ctrl Pts',(51.5884708356576,-2.19891818445906,340.492967265564));
#16079=CARTESIAN_POINT('Ctrl Pts',(51.5810721659029,-2.05272522570621,340.55149052629));
#16080=CARTESIAN_POINT('Ctrl Pts',(51.5736734961481,-1.90411578824837,340.604204889221));
#16081=CARTESIAN_POINT('Ctrl Pts',(51.5662748263934,-1.75359344334423,340.65091502307));
#16082=CARTESIAN_POINT('Ctrl Pts',(51.5588773771894,-1.60309592995303,340.697617451198));
#16083=CARTESIAN_POINT('Ctrl Pts',(51.5514799279855,-1.45068649151728,340.738317505586));
#16084=CARTESIAN_POINT('Ctrl Pts',(51.5440824787815,-1.29688560543285,340.772869155708));
#16085=CARTESIAN_POINT('Ctrl Pts',(51.5366853503181,-1.1430913878867,340.80741930773));
#16086=CARTESIAN_POINT('Ctrl Pts',(51.5292882218546,-0.987906206784983,
340.835821503739));
#16087=CARTESIAN_POINT('Ctrl Pts',(51.5218910933911,-0.831862262539577,
340.857980517095));
#16088=CARTESIAN_POINT('Ctrl Pts',(51.5144928259545,-0.675794291421915,
340.880142942385));
#16089=CARTESIAN_POINT('Ctrl Pts',(51.5070945585179,-0.518867663403791,
340.896060218484));
#16090=CARTESIAN_POINT('Ctrl Pts',(51.4996962910813,-0.36162110806051,340.905688845233));
#16091=CARTESIAN_POINT('Ctrl Pts',(51.4922954245555,-0.204319310347798,
340.915320854619));
#16092=CARTESIAN_POINT('Ctrl Pts',(51.4848945580297,-0.0466977338128898,
340.918659793208));
#16093=CARTESIAN_POINT('Ctrl Pts',(51.477493691504,0.110703624027263,340.915714265423));
#16094=CARTESIAN_POINT('Ctrl Pts',(51.4700846981192,0.268277823605588,340.912765503166));
#16095=CARTESIAN_POINT('Ctrl Pts',(51.4626757047345,0.425630948190814,340.903518499966));
#16096=CARTESIAN_POINT('Ctrl Pts',(51.4552667113497,0.582226121880862,340.888033908318));
#16097=CARTESIAN_POINT('Ctrl Pts',(51.4478531537695,0.738917763599223,340.872539777627));
#16098=CARTESIAN_POINT('Ctrl Pts',(51.4404395961892,0.8948501552421,340.850800453072));
#16099=CARTESIAN_POINT('Ctrl Pts',(51.433026038609,1.04949587479265,340.822927869319));
#16100=CARTESIAN_POINT('Ctrl Pts',(51.4256019264723,1.20436176083678,340.795015603841));
#16101=CARTESIAN_POINT('Ctrl Pts',(51.4181778143357,1.35793695291711,340.760952720575));
#16102=CARTESIAN_POINT('Ctrl Pts',(51.410753702199,1.50970766647115,340.72090144333));
#16103=CARTESIAN_POINT('Ctrl Pts',(51.4068965770443,1.58855866255312,340.70009319231));
#16104=CARTESIAN_POINT('Ctrl Pts',(51.4030394518895,1.66692288412385,340.677669348726));
#16105=CARTESIAN_POINT('Ctrl Pts',(51.3991823267348,1.74473044719056,340.653657774322));
#16106=CARTESIAN_POINT('Ctrl Pts',(51.3917583492968,1.89449006595895,340.60744164716));
#16107=CARTESIAN_POINT('Ctrl Pts',(51.3843343718587,2.04263800935645,340.555201222443));
#16108=CARTESIAN_POINT('Ctrl Pts',(51.3769103944207,2.18865285682813,340.497065511234));
#16109=CARTESIAN_POINT('Ctrl Pts',(51.3694951783931,2.33449538481078,340.438998408911));
#16110=CARTESIAN_POINT('Ctrl Pts',(51.3620799623654,2.478209484374,340.375050005474));
#16111=CARTESIAN_POINT('Ctrl Pts',(51.3546647463378,2.61928762522662,340.305399409925));
#16112=CARTESIAN_POINT('Ctrl Pts',(51.3472566651937,2.76023002140195,340.235815831829));
#16113=CARTESIAN_POINT('Ctrl Pts',(51.3398485840496,2.89854117576706,340.160541148573));
#16114=CARTESIAN_POINT('Ctrl Pts',(51.3324405029055,3.0337324322031,340.079802958019));
#16115=CARTESIAN_POINT('Ctrl Pts',(51.3250379357315,3.16882306331819,339.999124862375));
#16116=CARTESIAN_POINT('Ctrl Pts',(51.3176353685574,3.30079810129,339.912991547142));
#16117=CARTESIAN_POINT('Ctrl Pts',(51.3102328013834,3.4291925574252,339.821676986962));
#16118=CARTESIAN_POINT('Ctrl Pts',(51.3028341316286,3.55751941444094,339.730410503499));
#16119=CARTESIAN_POINT('Ctrl Pts',(51.2954354618739,3.68226914065808,339.633968423628));
#16120=CARTESIAN_POINT('Ctrl Pts',(51.2880367921191,3.80300496652803,339.532668506196));
#16121=CARTESIAN_POINT('Ctrl Pts',(51.2806393429151,3.92372087473515,339.431385300106));
#16122=CARTESIAN_POINT('Ctrl Pts',(51.273241893711,4.04042391115701,339.32524608661));
#16123=CARTESIAN_POINT('Ctrl Pts',(51.2658444445071,4.15270961542479,339.214609520757));
#16124=CARTESIAN_POINT('Ctrl Pts',(51.2584473160436,4.26499045118042,339.103977751913));
#16125=CARTESIAN_POINT('Ctrl Pts',(51.2510501875801,4.3728540697571,338.988849280371));
#16126=CARTESIAN_POINT('Ctrl Pts',(51.2436530591166,4.47593238886079,338.869620112213));
#16127=CARTESIAN_POINT('Ctrl Pts',(51.23625479168,4.57902657945222,338.75037258574));
#16128=CARTESIAN_POINT('Ctrl Pts',(51.2288565242434,4.67733375937255,338.627023387787));
#16129=CARTESIAN_POINT('Ctrl Pts',(51.2214582568068,4.77052581092442,338.500002007114));
#16130=CARTESIAN_POINT('Ctrl Pts',(51.214057390281,4.8637506018245,338.372936002494));
#16131=CARTESIAN_POINT('Ctrl Pts',(51.2066565237552,4.95185646590455,338.242195547336));
#16132=CARTESIAN_POINT('Ctrl Pts',(51.1992556572294,5.03455841516474,338.108239393418));
#16133=CARTESIAN_POINT('Ctrl Pts',(51.1918466638446,5.11735117907148,337.974136142837));
#16134=CARTESIAN_POINT('Ctrl Pts',(51.1844376704598,5.19472798143771,337.836810459366));
#16135=CARTESIAN_POINT('Ctrl Pts',(51.177028677075,5.26644929188387,337.696746635952));
#16136=CARTESIAN_POINT('Ctrl Pts',(51.1696151194948,5.33821478513126,337.55659652839));
#16137=CARTESIAN_POINT('Ctrl Pts',(51.1622015619145,5.40431768784139,337.413705257666));
#16138=CARTESIAN_POINT('Ctrl Pts',(51.1547880043343,5.46456670994654,337.268576918476));
#16139=CARTESIAN_POINT('Ctrl Pts',(51.1473638921976,5.52490150756467,337.123241962527));
#16140=CARTESIAN_POINT('Ctrl Pts',(51.1399397800609,5.579365650904,336.97566392646));
#16141=CARTESIAN_POINT('Ctrl Pts',(51.1325156679242,5.62781751911758,336.826362651286));
#16142=CARTESIAN_POINT('Ctrl Pts',(51.1286585427697,5.65299021535728,336.74879462787));
#16143=CARTESIAN_POINT('Ctrl Pts',(51.1248014176153,5.67654090372352,336.670761653686));
#16144=CARTESIAN_POINT('Ctrl Pts',(51.1209442924608,5.69845519551331,336.592337573264));
#16145=CARTESIAN_POINT('Ctrl Pts',(51.1135203150228,5.74063459112599,336.441391316573));
#16146=CARTESIAN_POINT('Ctrl Pts',(51.1060963375848,5.77687585638018,336.288540259003));
#16147=CARTESIAN_POINT('Ctrl Pts',(51.0986723601468,5.80700530885049,336.134292689513));
#16148=CARTESIAN_POINT('Ctrl Pts',(51.0912571441192,5.83709920403371,335.980227155362));
#16149=CARTESIAN_POINT('Ctrl Pts',(51.0838419280915,5.86109557289093,335.824768752575));
#16150=CARTESIAN_POINT('Ctrl Pts',(51.0764267120639,5.87887037824104,335.668441200361));
#16151=CARTESIAN_POINT('Ctrl Pts',(51.0690186309198,5.89662808076293,335.51226406573));
#16152=CARTESIAN_POINT('Ctrl Pts',(51.0616105497757,5.9081760956172,335.355219814915));
#16153=CARTESIAN_POINT('Ctrl Pts',(51.0542024686316,5.91344137483696,335.197842535534));
#16154=CARTESIAN_POINT('Ctrl Pts',(51.0467999014575,5.91870273501325,335.040582394935));
#16155=CARTESIAN_POINT('Ctrl Pts',(51.0393973342835,5.91769065843273,334.882990090739));
#16156=CARTESIAN_POINT('Ctrl Pts',(51.0319947671094,5.91038390415388,334.725604905257));
#16157=CARTESIAN_POINT('Ctrl Pts',(51.0245960973547,5.90308099684926,334.568302582389));
#16158=CARTESIAN_POINT('Ctrl Pts',(51.0171974276,5.88949002937804,334.411207532932));
#16159=CARTESIAN_POINT('Ctrl Pts',(51.0097987578452,5.86964185086974,334.254859003263));
#16160=CARTESIAN_POINT('Ctrl Pts',(51.0024013086412,5.84979694669454,334.098536266246));
#16161=CARTESIAN_POINT('Ctrl Pts',(50.9950038594373,5.82369692711172,333.94296017448));
#16162=CARTESIAN_POINT('Ctrl Pts',(50.9876064102333,5.79142451609014,333.788664936143));
#16163=CARTESIAN_POINT('Ctrl Pts',(50.9802092817698,5.75915350434404,333.634376387778));
#16164=CARTESIAN_POINT('Ctrl Pts',(50.9728121533063,5.72071070969162,333.481368947727));
#16165=CARTESIAN_POINT('Ctrl Pts',(50.9654150248428,5.67622995164501,333.330166445855));
#16166=CARTESIAN_POINT('Ctrl Pts',(50.9580167574062,5.63174234467205,333.178940662573));
#16167=CARTESIAN_POINT('Ctrl Pts',(50.9506184899696,5.58121502849314,333.029520728898));
#16168=CARTESIAN_POINT('Ctrl Pts',(50.943220222533,5.52483160605675,332.882414987016));
#16169=CARTESIAN_POINT('Ctrl Pts',(50.9358193560073,5.46842837553104,332.735257565339));
#16170=CARTESIAN_POINT('Ctrl Pts',(50.9284184894815,5.40616507613066,332.590416302406));
#16171=CARTESIAN_POINT('Ctrl Pts',(50.9210176229557,5.33827325865388,332.448379107618));
#16172=CARTESIAN_POINT('Ctrl Pts',(50.913608629571,5.2703068894709,332.30618594241));
#16173=CARTESIAN_POINT('Ctrl Pts',(50.9061996361862,5.19669982016629,332.166803331467));
#16174=CARTESIAN_POINT('Ctrl Pts',(50.8987906428014,5.11772967937687,332.030694779696));
#16175=CARTESIAN_POINT('Ctrl Pts',(50.8913770852212,5.03871089025671,331.894502380362));
#16176=CARTESIAN_POINT('Ctrl Pts',(50.8839635276409,4.9543226458939,331.761588373541));
#16177=CARTESIAN_POINT('Ctrl Pts',(50.8765499700607,4.86488533224153,331.632386413699));
#16178=CARTESIAN_POINT('Ctrl Pts',(50.869125857924,4.77532068819956,331.503000511213));
#16179=CARTESIAN_POINT('Ctrl Pts',(50.8617017457873,4.68069284234474,331.377337507796));
#16180=CARTESIAN_POINT('Ctrl Pts',(50.8542776336506,4.58136230090664,331.255797811238));
#16181=CARTESIAN_POINT('Ctrl Pts',(50.8504205084961,4.52975608551756,331.192653045609));
#16182=CARTESIAN_POINT('Ctrl Pts',(50.8465633833414,4.47688112157734,331.130620649466));
#16183=CARTESIAN_POINT('Ctrl Pts',(50.8427062581869,4.4227917199731,331.069752684088));
#16184=CARTESIAN_POINT('Ctrl Pts',(50.8352822807489,4.31868348364384,330.952597449669));
#16185=CARTESIAN_POINT('Ctrl Pts',(50.8278583033109,4.2097599965518,330.839404918701));
#16186=CARTESIAN_POINT('Ctrl Pts',(50.8204343258729,4.09635470019938,330.73059620876));
#16187=CARTESIAN_POINT('Ctrl Pts',(50.8130191098453,3.98308323915932,330.621915909468));
#16188=CARTESIAN_POINT('Ctrl Pts',(50.8056038938176,3.86534076379671,330.517609389007));
#16189=CARTESIAN_POINT('Ctrl Pts',(50.79818867779,3.74350055713083,330.418064367403));
#16190=CARTESIAN_POINT('Ctrl Pts',(50.7907805966459,3.62177758449868,330.318615127518));
#16191=CARTESIAN_POINT('Ctrl Pts',(50.7833725155019,3.49596501705927,330.223918500148));
#16192=CARTESIAN_POINT('Ctrl Pts',(50.7759644343578,3.36647245003869,330.134324938343));
#16193=CARTESIAN_POINT('Ctrl Pts',(50.7685618671839,3.23707626670113,330.044798062663));
#16194=CARTESIAN_POINT('Ctrl Pts',(50.7611593000099,3.10400584330925,329.960366901007));
#16195=CARTESIAN_POINT('Ctrl Pts',(50.7537567328359,2.96770317917187,329.881341151939));
#16196=CARTESIAN_POINT('Ctrl Pts',(50.7463580630812,2.83147227778989,329.802357009582));
#16197=CARTESIAN_POINT('Ctrl Pts',(50.7389593933264,2.69201284687648,329.728772798705));
#16198=CARTESIAN_POINT('Ctrl Pts',(50.7315607235716,2.54979504444844,329.660854394774));
#16199=CARTESIAN_POINT('Ctrl Pts',(50.7241632743677,2.40760070354261,329.592947195271));
#16200=CARTESIAN_POINT('Ctrl Pts',(50.7167658251636,2.26264923069101,329.530704108348));
#16201=CARTESIAN_POINT('Ctrl Pts',(50.7093683759597,2.11543461963498,329.474344660355));
#16202=CARTESIAN_POINT('Ctrl Pts',(50.7019712474962,1.96822639154762,329.417987656009));
#16203=CARTESIAN_POINT('Ctrl Pts',(50.6945741190328,1.8187555689043,329.367513916796));
#16204=CARTESIAN_POINT('Ctrl Pts',(50.6871769905693,1.66753506883221,329.323094385432));
#16205=CARTESIAN_POINT('Ctrl Pts',(50.6797787231327,1.51629128457905,329.278668014569));
#16206=CARTESIAN_POINT('Ctrl Pts',(50.6723804556962,1.36329764457743,329.240297812872));
#16207=CARTESIAN_POINT('Ctrl Pts',(50.6649821882596,1.2090809827058,329.208104477828));
#16208=CARTESIAN_POINT('Ctrl Pts',(50.6575813217338,1.0548101428972,329.175899832926));
#16209=CARTESIAN_POINT('Ctrl Pts',(50.650180455208,0.899315790871016,329.149876451358));
#16210=CARTESIAN_POINT('Ctrl Pts',(50.6427795886822,0.743133525473775,329.13010365289));
#16211=CARTESIAN_POINT('Ctrl Pts',(50.6353705952975,0.586779757018519,329.110309141999));
#16212=CARTESIAN_POINT('Ctrl Pts',(50.6279616019127,0.429736937105505,329.096778968361));
#16213=CARTESIAN_POINT('Ctrl Pts',(50.620552608528,0.272545077685719,329.089530497234));
#16214=CARTESIAN_POINT('Ctrl Pts',(50.6131390509477,0.115256382657845,329.082277560799));
#16215=CARTESIAN_POINT('Ctrl Pts',(50.6057254933675,-0.0421811624949565,
329.081314040133));
#16216=CARTESIAN_POINT('Ctrl Pts',(50.5983119357873,-0.199229509259026,
329.086605191166));
#16217=CARTESIAN_POINT('Ctrl Pts',(50.5908878236506,-0.356501443095588,
329.091903875122));
#16218=CARTESIAN_POINT('Ctrl Pts',(50.5834637115139,-0.513382700708155,
329.103474987807));
#16219=CARTESIAN_POINT('Ctrl Pts',(50.5760395993772,-0.669341480036475,
329.121232055473));
#16220=CARTESIAN_POINT('Ctrl Pts',(50.5721824742225,-0.750368344902806,
329.130457567036));
#16221=CARTESIAN_POINT('Ctrl Pts',(50.5683253490677,-0.831146387179152,
329.141351963281));
#16222=CARTESIAN_POINT('Ctrl Pts',(50.564468223913,-0.911602436687748,329.153897746368));
#16223=CARTESIAN_POINT('Ctrl Pts',(50.557044246475,-1.06645971311497,329.178045163639));
#16224=CARTESIAN_POINT('Ctrl Pts',(50.549620269037,-1.22059047615725,329.208386274223));
#16225=CARTESIAN_POINT('Ctrl Pts',(50.542196291599,-1.37346015472957,329.24486857093));
#16226=CARTESIAN_POINT('Ctrl Pts',(50.5347810755714,-1.52614942408015,329.281307813038));
#16227=CARTESIAN_POINT('Ctrl Pts',(50.5273658595438,-1.67758021189812,329.323873729168));
#16228=CARTESIAN_POINT('Ctrl Pts',(50.5199506435162,-1.82722447128094,329.372462235218));
#16229=CARTESIAN_POINT('Ctrl Pts',(50.5125425623721,-1.97672474371095,329.421003989652));
#16230=CARTESIAN_POINT('Ctrl Pts',(50.505134481228,-2.12444155729559,329.475556682944));
#16231=CARTESIAN_POINT('Ctrl Pts',(50.4977264000839,-2.26985855310917,329.535965527984));
#16232=CARTESIAN_POINT('Ctrl Pts',(50.4903238329099,-2.41516731239723,329.596329409618));
#16233=CARTESIAN_POINT('Ctrl Pts',(50.4829212657359,-2.55817931917107,329.662540621351));
#16234=CARTESIAN_POINT('Ctrl Pts',(50.4755186985619,-2.69839495011332,329.734395072197));
#16235=CARTESIAN_POINT('Ctrl Pts',(50.4681200288071,-2.83853675813838,329.806211691989));
#16236=CARTESIAN_POINT('Ctrl Pts',(50.4607213590524,-2.97588479116169,329.883665463913));
#16237=CARTESIAN_POINT('Ctrl Pts',(50.4533226892977,-3.10996103935167,329.966504902534));
#16238=CARTESIAN_POINT('Ctrl Pts',(50.4459252400937,-3.24401516912417,330.049330675219));
#16239=CARTESIAN_POINT('Ctrl Pts',(50.4385277908898,-3.37479826808915,330.137540155303));
#16240=CARTESIAN_POINT('Ctrl Pts',(50.4311303416858,-3.50185840349794,330.230836731213));
#16241=CARTESIAN_POINT('Ctrl Pts',(50.4237332132223,-3.6289130298004,330.324129261945));
#16242=CARTESIAN_POINT('Ctrl Pts',(50.4163360847588,-3.75224471268036,330.422508229055));
#16243=CARTESIAN_POINT('Ctrl Pts',(50.4089389562954,-3.87143213387249,330.5256348165));
#16244=CARTESIAN_POINT('Ctrl Pts',(50.4015406888588,-3.99063790695293,330.628777282865));
#16245=CARTESIAN_POINT('Ctrl Pts',(50.3941424214222,-4.10569786553179,330.7366685809));
#16246=CARTESIAN_POINT('Ctrl Pts',(50.3867441539855,-4.21622541247485,330.848931001091));
#16247=CARTESIAN_POINT('Ctrl Pts',(50.3793432874598,-4.32679178890742,330.961232860252));
#16248=CARTESIAN_POINT('Ctrl Pts',(50.371942420934,-4.43282232179738,331.077908633209));
#16249=CARTESIAN_POINT('Ctrl Pts',(50.3645415544083,-4.53396887540603,331.198545436369));
#16250=CARTESIAN_POINT('Ctrl Pts',(50.3571325610235,-4.63522649760047,331.319314710273));
#16251=CARTESIAN_POINT('Ctrl Pts',(50.3497235676387,-4.73158919023638,331.444053414583));
#16252=CARTESIAN_POINT('Ctrl Pts',(50.342314574254,-4.82275011904547,331.572316839067));
#16253=CARTESIAN_POINT('Ctrl Pts',(50.3349010166737,-4.91396720613118,331.700659278244));
#16254=CARTESIAN_POINT('Ctrl Pts',(50.3274874590935,-4.99997594066146,331.832530452426));
#16255=CARTESIAN_POINT('Ctrl Pts',(50.3200739015133,-5.08051437074151,331.96745910313));
#16256=CARTESIAN_POINT('Ctrl Pts',(50.3126497893766,-5.16116746202119,332.10257984947));
#16257=CARTESIAN_POINT('Ctrl Pts',(50.3052256772399,-5.23633451684443,332.240766438935));
#16258=CARTESIAN_POINT('Ctrl Pts',(50.2978015651032,-5.3058004642216,332.381524871921));
#16259=CARTESIAN_POINT('Ctrl Pts',(50.2939444399485,-5.34189082062931,332.454654544886));
#16260=CARTESIAN_POINT('Ctrl Pts',(50.2900873147938,-5.37644312412405,332.528478106887));
#16261=CARTESIAN_POINT('Ctrl Pts',(50.2862301896391,-5.40943249242955,332.602924558478));
#16262=CARTESIAN_POINT('Ctrl Pts',(50.2780661846716,-5.47925790797001,332.760498185523));
#16263=CARTESIAN_POINT('Ctrl Pts',(50.2699021797042,-5.54225998356434,332.921272647656));
#16264=CARTESIAN_POINT('Ctrl Pts',(50.2617381747368,-5.59816281199632,333.084666166727));
#16265=CARTESIAN_POINT('Ctrl Pts',(50.2536045243065,-5.653857788462,333.247452173348));
#16266=CARTESIAN_POINT('Ctrl Pts',(50.2454708738763,-5.70250608800867,333.412837577739));
#16267=CARTESIAN_POINT('Ctrl Pts',(50.237337223446,-5.74388052029439,333.580222858656));
#16268=CARTESIAN_POINT('Ctrl Pts',(50.2292225881197,-5.78515822613071,333.747216820998));
#16269=CARTESIAN_POINT('Ctrl Pts',(50.2211079527933,-5.81919591411558,333.916201097296));
#16270=CARTESIAN_POINT('Ctrl Pts',(50.2129933174669,-5.84581534515739,334.08655951873));
#16271=CARTESIAN_POINT('Ctrl Pts',(50.2049101411301,-5.87233157742681,334.256257491039));
#16272=CARTESIAN_POINT('Ctrl Pts',(50.1968269647934,-5.8914868647934,334.427318739594));
#16273=CARTESIAN_POINT('Ctrl Pts',(50.1887437884566,-5.90315367809505,334.599116955593));
#16274=CARTESIAN_POINT('Ctrl Pts',(50.1825132123242,-5.91214654989078,334.731540376734));
#16275=CARTESIAN_POINT('Ctrl Pts',(50.1762826361917,-5.91669114572374,334.864401284286));
#16276=CARTESIAN_POINT('Ctrl Pts',(50.1700520600592,-5.91674943187699,334.997407147659));
#16277=CARTESIAN_POINT('',(48.4200519872132,-5.9145671363793,335.005177061859));
#16278=CARTESIAN_POINT('Ctrl Pts',(50.1700520047037,-5.9080523696217,334.99741213886));
#16279=CARTESIAN_POINT('Ctrl Pts',(50.1160320549241,-5.90352393792915,336.148898367647));
#16280=CARTESIAN_POINT('Ctrl Pts',(49.96926609372,-5.02192580754506,339.283759072858));
#16281=CARTESIAN_POINT('Ctrl Pts',(49.729754121091,0.0702832997843916,341.996262086213));
#16282=CARTESIAN_POINT('Ctrl Pts',(49.4515160868174,5.92134037336825,338.726976134069));
#16283=CARTESIAN_POINT('Ctrl Pts',(49.1732780525432,6.33847078515738,332.037499193767));
#16284=CARTESIAN_POINT('Ctrl Pts',(48.8950400182694,0.938880113080063,328.066665516904));
#16285=CARTESIAN_POINT('Ctrl Pts',(48.6439646689894,-4.71106541156814,330.224955150084));
#16286=CARTESIAN_POINT('Ctrl Pts',(48.4856353311342,-5.90162062968873,333.610301631254));
#16287=CARTESIAN_POINT('Ctrl Pts',(48.4200520047037,-5.91326451545619,335.005175549532));
#16288=CARTESIAN_POINT('',(46.6700520047037,-5.92206232538312,335.000121321822));
#16289=CARTESIAN_POINT('Ctrl Pts',(48.4200519579342,-5.91674773286061,335.005179593505));
#16290=CARTESIAN_POINT('Ctrl Pts',(48.4110676566621,-5.91658035782511,335.196375265698));
#16291=CARTESIAN_POINT('Ctrl Pts',(48.40208335539,-5.90714176842452,335.387163876296));
#16292=CARTESIAN_POINT('Ctrl Pts',(48.3930990541179,-5.88857245527102,335.576753848295));
#16293=CARTESIAN_POINT('Ctrl Pts',(48.3839905901862,-5.86974651500326,335.768963945606));
#16294=CARTESIAN_POINT('Ctrl Pts',(48.3748821262545,-5.84153578648773,335.959942063276));
#16295=CARTESIAN_POINT('Ctrl Pts',(48.3657736623228,-5.80413574004996,336.148885927138));
#16296=CARTESIAN_POINT('Ctrl Pts',(48.3567037581224,-5.76689402280502,336.337029916873));
#16297=CARTESIAN_POINT('Ctrl Pts',(48.347633853922,-5.72054076236795,336.523156929097));
#16298=CARTESIAN_POINT('Ctrl Pts',(48.3385639497216,-5.6653156537755,336.706496148717));
#16299=CARTESIAN_POINT('Ctrl Pts',(48.3311399722836,-5.62011231412162,336.856564572802));
#16300=CARTESIAN_POINT('Ctrl Pts',(48.3237159948457,-5.5688739263724,337.005062056713));
#16301=CARTESIAN_POINT('Ctrl Pts',(48.3162920174077,-5.5117259760806,337.151466320233));
#16302=CARTESIAN_POINT('Ctrl Pts',(48.3088768013801,-5.45464546896845,337.297697804695));
#16303=CARTESIAN_POINT('Ctrl Pts',(48.3014615853525,-5.39166941590445,337.441840641686));
#16304=CARTESIAN_POINT('Ctrl Pts',(48.2940463693249,-5.3229734930756,337.583386102485));
#16305=CARTESIAN_POINT('Ctrl Pts',(48.2866382881809,-5.25434366911781,337.724795368956));
#16306=CARTESIAN_POINT('Ctrl Pts',(48.2792302070368,-5.18000509395967,337.863611901128));
#16307=CARTESIAN_POINT('Ctrl Pts',(48.2718221258927,-5.10018205904981,337.99934551645));
#16308=CARTESIAN_POINT('Ctrl Pts',(48.2644195587187,-5.02041843788275,338.134978102762));
#16309=CARTESIAN_POINT('Ctrl Pts',(48.2570169915448,-4.93517867356555,338.267532020922));
#16310=CARTESIAN_POINT('Ctrl Pts',(48.2496144243708,-4.84473359315843,338.396540441953));
#16311=CARTESIAN_POINT('Ctrl Pts',(48.2422157546161,-4.75433613169079,338.525480940614));
#16312=CARTESIAN_POINT('Ctrl Pts',(48.2348170848613,-4.65873902585754,338.650879354946));
#16313=CARTESIAN_POINT('Ctrl Pts',(48.2274184151066,-4.55825707656579,338.77229677868));
#16314=CARTESIAN_POINT('Ctrl Pts',(48.2200209659027,-4.45779170367561,338.893694172309));
#16315=CARTESIAN_POINT('Ctrl Pts',(48.2126235166987,-4.35244332438794,339.011111591514));
#16316=CARTESIAN_POINT('Ctrl Pts',(48.2052260674948,-4.24256785314958,339.124142162186));
#16317=CARTESIAN_POINT('Ctrl Pts',(48.1978289390313,-4.1326971459201,339.23716783205));
#16318=CARTESIAN_POINT('Ctrl Pts',(48.1904318105679,-4.01829999716163,339.345806763964));
#16319=CARTESIAN_POINT('Ctrl Pts',(48.1830346821044,-3.8997699172604,339.449688208732));
#16320=CARTESIAN_POINT('Ctrl Pts',(48.1756364146678,-3.78122158668578,339.553585648649));
#16321=CARTESIAN_POINT('Ctrl Pts',(48.1682381472313,-3.65853933856589,339.652723896846));
#16322=CARTESIAN_POINT('Ctrl Pts',(48.1608398797947,-3.53215043519213,339.746771941612));
#16323=CARTESIAN_POINT('Ctrl Pts',(48.153439013269,-3.40571713006748,339.840853026444));
#16324=CARTESIAN_POINT('Ctrl Pts',(48.1460381467432,-3.27557487626077,339.9298401248));
#16325=CARTESIAN_POINT('Ctrl Pts',(48.1386372802175,-3.14218048978496,340.01344515599));
#16326=CARTESIAN_POINT('Ctrl Pts',(48.1312282868328,-3.00863962351961,340.097141993496));
#16327=CARTESIAN_POINT('Ctrl Pts',(48.123819293448,-2.87183980922479,340.175444762883));
#16328=CARTESIAN_POINT('Ctrl Pts',(48.1164103000633,-2.73226371059572,340.248110667494));
#16329=CARTESIAN_POINT('Ctrl Pts',(48.1089967424831,-2.5926016282755,340.320821336808));
#16330=CARTESIAN_POINT('Ctrl Pts',(48.1015831849028,-2.45016019051551,340.387888063315));
#16331=CARTESIAN_POINT('Ctrl Pts',(48.0941696273226,-2.30544218820852,340.449116155793));
#16332=CARTESIAN_POINT('Ctrl Pts',(48.0867455151859,-2.16051815333116,340.510431417671));
#16333=CARTESIAN_POINT('Ctrl Pts',(48.0793214030493,-2.01331142907448,340.565891312841));
#16334=CARTESIAN_POINT('Ctrl Pts',(48.0718972909127,-1.86434088783647,340.615350711794));
#16335=CARTESIAN_POINT('Ctrl Pts',(48.0680401657576,-1.78694469400318,340.64104686082));
#16336=CARTESIAN_POINT('Ctrl Pts',(48.0641830406026,-1.70907260219412,340.665124180061));
#16337=CARTESIAN_POINT('Ctrl Pts',(48.0603259154475,-1.63079835804735,340.687567782268));
#16338=CARTESIAN_POINT('Ctrl Pts',(48.0529019380095,-1.48014049781042,340.730765964779));
#16339=CARTESIAN_POINT('Ctrl Pts',(48.0454779605715,-1.32753776386418,340.768039020726));
#16340=CARTESIAN_POINT('Ctrl Pts',(48.0380539831335,-1.173497260219,340.799209837793));
#16341=CARTESIAN_POINT('Ctrl Pts',(48.0306387671058,-1.01963854754477,340.830343868607));
#16342=CARTESIAN_POINT('Ctrl Pts',(48.0232235510782,-0.864345804888217,
340.85538992206));
#16343=CARTESIAN_POINT('Ctrl Pts',(48.0158083350505,-0.70814190154676,340.874220425705));
#16344=CARTESIAN_POINT('Ctrl Pts',(48.0084002539064,-0.552088296814716,
340.893032810735));
#16345=CARTESIAN_POINT('Ctrl Pts',(48.0009921727623,-0.395125644824597,
340.90564150779));
#16346=CARTESIAN_POINT('Ctrl Pts',(47.9935840916182,-0.237787527515724,
340.911969862428));
#16347=CARTESIAN_POINT('Ctrl Pts',(47.9861815244442,-0.0805665198410168,
340.918293506756));
#16348=CARTESIAN_POINT('Ctrl Pts',(47.9787789572701,0.0770290253830899,
340.918346101489));
#16349=CARTESIAN_POINT('Ctrl Pts',(47.9713763900961,0.234459981648922,340.912102762935));
#16350=CARTESIAN_POINT('Ctrl Pts',(47.9639777203413,0.391808051204665,340.905862711471));
#16351=CARTESIAN_POINT('Ctrl Pts',(47.9565790505866,0.548991332402498,340.893333343055));
#16352=CARTESIAN_POINT('Ctrl Pts',(47.9491803808318,0.705470382763265,340.87454186312));
#16353=CARTESIAN_POINT('Ctrl Pts',(47.9417829316278,0.861923618939321,340.855753483195));
#16354=CARTESIAN_POINT('Ctrl Pts',(47.9343854824238,1.01767248466195,340.830705086484));
#16355=CARTESIAN_POINT('Ctrl Pts',(47.9269880332198,1.1721822250829,340.799475786112));
#16356=CARTESIAN_POINT('Ctrl Pts',(47.9195909047563,1.32668526623088,340.768247839788));
#16357=CARTESIAN_POINT('Ctrl Pts',(47.9121937762928,1.47994892308881,340.7308395966));
#16358=CARTESIAN_POINT('Ctrl Pts',(47.9047966478293,1.63144847369738,340.687381334162));
#16359=CARTESIAN_POINT('Ctrl Pts',(47.8973983803927,1.7829713514548,340.643916380236));
#16360=CARTESIAN_POINT('Ctrl Pts',(47.8900001129561,1.93272922334991,340.594399655131));
#16361=CARTESIAN_POINT('Ctrl Pts',(47.8826018455195,2.08021251843005,340.539011323392));
#16362=CARTESIAN_POINT('Ctrl Pts',(47.8752009789937,2.22774762594272,340.48360353315));
#16363=CARTESIAN_POINT('Ctrl Pts',(47.867800112468,2.37300621650351,340.422320160459));
#16364=CARTESIAN_POINT('Ctrl Pts',(47.8603992459422,2.51549882755647,340.355389454658));
#16365=CARTESIAN_POINT('Ctrl Pts',(47.8529902525574,2.65814790911929,340.288385252543));
#16366=CARTESIAN_POINT('Ctrl Pts',(47.8455812591727,2.79802460750033,340.215721491733));
#16367=CARTESIAN_POINT('Ctrl Pts',(47.8381722657879,2.93466355279005,340.137672663223));
#16368=CARTESIAN_POINT('Ctrl Pts',(47.8307587082076,3.07138667238326,340.059575753942));
#16369=CARTESIAN_POINT('Ctrl Pts',(47.8233451506274,3.20486774876914,339.976087364074));
#16370=CARTESIAN_POINT('Ctrl Pts',(47.8159315930471,3.33467097294413,339.887524942617));
#16371=CARTESIAN_POINT('Ctrl Pts',(47.8085074809104,3.46465899577239,339.798836436339));
#16372=CARTESIAN_POINT('Ctrl Pts',(47.8010833687737,3.59095841002202,339.705059692958));
#16373=CARTESIAN_POINT('Ctrl Pts',(47.793659256637,3.71316638156332,339.606552505435));
#16374=CARTESIAN_POINT('Ctrl Pts',(47.7898021314825,3.7766583429496,339.555374055555));
#16375=CARTESIAN_POINT('Ctrl Pts',(47.7859450063281,3.83904653153453,339.502919371229));
#16376=CARTESIAN_POINT('Ctrl Pts',(47.7820878811736,3.90027852031823,339.449242410393));
#16377=CARTESIAN_POINT('Ctrl Pts',(47.7746639037356,4.0181344065045,339.345928016844));
#16378=CARTESIAN_POINT('Ctrl Pts',(47.7672399262975,4.13206021011723,339.237771711533));
#16379=CARTESIAN_POINT('Ctrl Pts',(47.7598159488595,4.24163257055394,339.125104083404));
#16380=CARTESIAN_POINT('Ctrl Pts',(47.7524007328319,4.35107561911929,339.012569420028));
#16381=CARTESIAN_POINT('Ctrl Pts',(47.7449855168043,4.45617519354885,338.895534296369));
#16382=CARTESIAN_POINT('Ctrl Pts',(47.7375703007767,4.55654106087152,338.774369367602));
#16383=CARTESIAN_POINT('Ctrl Pts',(47.7301622196326,4.656810356662,338.653321023119));
#16384=CARTESIAN_POINT('Ctrl Pts',(47.7227541384885,4.75235477651703,338.528151069873));
#16385=CARTESIAN_POINT('Ctrl Pts',(47.7153460573444,4.84282110827666,338.399266726182));
#16386=CARTESIAN_POINT('Ctrl Pts',(47.7079434901704,4.93322010429331,338.270478313462));
#16387=CARTESIAN_POINT('Ctrl Pts',(47.7005409229964,5.01854832467766,338.137981319358));
#16388=CARTESIAN_POINT('Ctrl Pts',(47.6931383558224,5.0984930919132,338.002215640858));
#16389=CARTESIAN_POINT('Ctrl Pts',(47.6857396860676,5.17839576857824,337.866521442394));
#16390=CARTESIAN_POINT('Ctrl Pts',(47.6783410163129,5.2529204480056,337.727562307692));
#16391=CARTESIAN_POINT('Ctrl Pts',(47.6709423465581,5.32179808454506,337.585806587862));
#16392=CARTESIAN_POINT('Ctrl Pts',(47.6635448973541,5.39066435841326,337.444074253324));
#16393=CARTESIAN_POINT('Ctrl Pts',(47.6561474481502,5.4538852753457,337.299546584645));
#16394=CARTESIAN_POINT('Ctrl Pts',(47.6487499989462,5.51123797672396,337.152716081237));
#16395=CARTESIAN_POINT('Ctrl Pts',(47.6413528704827,5.56858819138904,337.005891944143));
#16396=CARTESIAN_POINT('Ctrl Pts',(47.6339557420192,5.62007056061471,336.856765518481));
#16397=CARTESIAN_POINT('Ctrl Pts',(47.6265586135557,5.66551068046576,336.705848554834));
#16398=CARTESIAN_POINT('Ctrl Pts',(47.6191603461191,5.71095779696097,336.554908353741));
#16399=CARTESIAN_POINT('Ctrl Pts',(47.6117620786826,5.75036070401466,336.402177423098));
#16400=CARTESIAN_POINT('Ctrl Pts',(47.604363811246,5.78359514775494,336.248181769361));
#16401=CARTESIAN_POINT('Ctrl Pts',(47.5969629447202,5.81684126710482,336.094132015332));
#16402=CARTESIAN_POINT('Ctrl Pts',(47.5895620781944,5.84391452987427,335.938817018171));
#16403=CARTESIAN_POINT('Ctrl Pts',(47.5821612116687,5.8647419995275,335.782771896199));
#16404=CARTESIAN_POINT('Ctrl Pts',(47.5747522182839,5.88559233973358,335.626555421763));
#16405=CARTESIAN_POINT('Ctrl Pts',(47.5673432248992,5.90018314067225,335.469607591536));
#16406=CARTESIAN_POINT('Ctrl Pts',(47.5599342315144,5.90849338931678,335.312468287831));
#16407=CARTESIAN_POINT('Ctrl Pts',(47.5525206739342,5.91680875736113,335.155232180894));
#16408=CARTESIAN_POINT('Ctrl Pts',(47.5451071163539,5.91883585874994,334.997804737747));
#16409=CARTESIAN_POINT('Ctrl Pts',(47.5376935587736,5.9146058018589,334.840724229347));
#16410=CARTESIAN_POINT('Ctrl Pts',(47.530269446637,5.91036972270746,334.683420088086));
#16411=CARTESIAN_POINT('Ctrl Pts',(47.5228453345002,5.89985871866828,334.526464239412));
#16412=CARTESIAN_POINT('Ctrl Pts',(47.5154212223635,5.88315566881497,334.370389057441));
#16413=CARTESIAN_POINT('Ctrl Pts',(47.5115640972089,5.87447776194045,334.289301716718));
#16414=CARTESIAN_POINT('Ctrl Pts',(47.5077069720543,5.86412932749561,334.208451918402));
#16415=CARTESIAN_POINT('Ctrl Pts',(47.5038498468997,5.8521273686027,334.127912949213));
#16416=CARTESIAN_POINT('Ctrl Pts',(47.4964258694617,5.82902667353565,333.972896073645));
#16417=CARTESIAN_POINT('Ctrl Pts',(47.4890018920237,5.79972751838205,333.818563852076));
#16418=CARTESIAN_POINT('Ctrl Pts',(47.4815779145857,5.76427879772342,333.665451198114));
#16419=CARTESIAN_POINT('Ctrl Pts',(47.4741626985581,5.72887191188869,333.51251924012));
#16420=CARTESIAN_POINT('Ctrl Pts',(47.4667474825304,5.68732998990494,333.360804344895));
#16421=CARTESIAN_POINT('Ctrl Pts',(47.4593322665028,5.6397535461651,333.210835250454));
#16422=CARTESIAN_POINT('Ctrl Pts',(47.4519241853587,5.5922228802399,333.06101045552));
#16423=CARTESIAN_POINT('Ctrl Pts',(47.4445161042147,5.53866936409267,332.912928470562));
#16424=CARTESIAN_POINT('Ctrl Pts',(47.4371080230706,5.47924429292858,332.767106688418));
#16425=CARTESIAN_POINT('Ctrl Pts',(47.4297054558966,5.41986345293028,332.621393444089));
#16426=CARTESIAN_POINT('Ctrl Pts',(47.4223028887226,5.35461990007123,332.477937396985));
#16427=CARTESIAN_POINT('Ctrl Pts',(47.4149003215486,5.28371434536787,332.3372395378));
#16428=CARTESIAN_POINT('Ctrl Pts',(47.4075016517939,5.21284612212912,332.196615755424));
#16429=CARTESIAN_POINT('Ctrl Pts',(47.4001029820392,5.13632200145885,332.058747601318));
#16430=CARTESIAN_POINT('Ctrl Pts',(47.3927043122845,5.05439023375785,331.924114773371));
#16431=CARTESIAN_POINT('Ctrl Pts',(47.3853068630805,4.9724719822544,331.78950415566));
#16432=CARTESIAN_POINT('Ctrl Pts',(47.3779094138765,4.88514804806749,331.658128123334));
#16433=CARTESIAN_POINT('Ctrl Pts',(47.3705119646725,4.79271198287325,331.530440602652));
#16434=CARTESIAN_POINT('Ctrl Pts',(47.3631148362091,4.70027992554565,331.402758618279));
#16435=CARTESIAN_POINT('Ctrl Pts',(47.3557177077456,4.60273639677976,331.278765129871));
#16436=CARTESIAN_POINT('Ctrl Pts',(47.3483205792821,4.50041735858163,331.158883735022));
#16437=CARTESIAN_POINT('Ctrl Pts',(47.3409223118455,4.39808256580584,331.038983881432));
#16438=CARTESIAN_POINT('Ctrl Pts',(47.333524044409,4.29097104180144,330.923197665996));
#16439=CARTESIAN_POINT('Ctrl Pts',(47.3261257769724,4.17945787572152,330.811914228723));
#16440=CARTESIAN_POINT('Ctrl Pts',(47.3187249104466,4.06790553389365,330.700591696409));
#16441=CARTESIAN_POINT('Ctrl Pts',(47.3113240439209,3.95194873522945,330.593775355227));
#16442=CARTESIAN_POINT('Ctrl Pts',(47.3039231773951,3.83199800199564,330.491816122295));
#16443=CARTESIAN_POINT('Ctrl Pts',(47.2965141840104,3.71191555138892,330.389744928377));
#16444=CARTESIAN_POINT('Ctrl Pts',(47.2891051906257,3.58783069222419,330.292541735986));
#16445=CARTESIAN_POINT('Ctrl Pts',(47.2816961972409,3.46018605170202,330.200516376723));
#16446=CARTESIAN_POINT('Ctrl Pts',(47.2742826396607,3.33246277767837,330.108434326664));
#16447=CARTESIAN_POINT('Ctrl Pts',(47.2668690820805,3.20117566304607,330.021536671188));
#16448=CARTESIAN_POINT('Ctrl Pts',(47.2594555245003,3.06679418586286,329.940088539899));
#16449=CARTESIAN_POINT('Ctrl Pts',(47.2520314123636,2.93222139204506,329.858524452284));
#16450=CARTESIAN_POINT('Ctrl Pts',(47.2446073002269,2.79454576298211,329.782425563981));
#16451=CARTESIAN_POINT('Ctrl Pts',(47.2371831880902,2.65425983404841,329.71201027839));
#16452=CARTESIAN_POINT('Ctrl Pts',(47.2333260629354,2.58137564596042,329.675426702558));
#16453=CARTESIAN_POINT('Ctrl Pts',(47.2294689377806,2.50778719402751,329.640376456826));
#16454=CARTESIAN_POINT('Ctrl Pts',(47.2256118126258,2.43356530797972,329.606884902554));
#16455=CARTESIAN_POINT('Ctrl Pts',(47.2181878351878,2.29070719855655,329.542422243632));
#16456=CARTESIAN_POINT('Ctrl Pts',(47.2107638577498,2.1450704868661,329.483542507598));
#16457=CARTESIAN_POINT('Ctrl Pts',(47.2033398803118,1.9971314528381,329.430494050404));
#16458=CARTESIAN_POINT('Ctrl Pts',(47.1959246642841,1.84936700912889,329.377508198371));
#16459=CARTESIAN_POINT('Ctrl Pts',(47.1885094482565,1.69930599937836,329.33034005162));
#16460=CARTESIAN_POINT('Ctrl Pts',(47.1810942322289,1.54744744476871,329.289191215933));
#16461=CARTESIAN_POINT('Ctrl Pts',(47.1736861510848,1.3957350076958,329.248081973448));
#16462=CARTESIAN_POINT('Ctrl Pts',(47.1662780699407,1.24222882686587,329.212980608687));
#16463=CARTESIAN_POINT('Ctrl Pts',(47.1588699887966,1.08744586347258,329.184039885237));
#16464=CARTESIAN_POINT('Ctrl Pts',(47.1514674216226,0.932778107865729,329.155120702896));
#16465=CARTESIAN_POINT('Ctrl Pts',(47.1440648544486,0.776835827228476,329.132353099811));
#16466=CARTESIAN_POINT('Ctrl Pts',(47.1366622872746,0.620148931572908,329.115839408618));
#16467=CARTESIAN_POINT('Ctrl Pts',(47.1292636175198,0.463544530882996,329.099334411812));
#16468=CARTESIAN_POINT('Ctrl Pts',(47.1218649477651,0.306196666159692,329.089076808395));
#16469=CARTESIAN_POINT('Ctrl Pts',(47.1144662780104,0.148643068126189,329.08511743136));
#16470=CARTESIAN_POINT('Ctrl Pts',(47.1070688288064,-0.00888453845582626,
329.0811587075));
#16471=CARTESIAN_POINT('Ctrl Pts',(47.0996713796024,-0.166617438258161,
329.083496157286));
#16472=CARTESIAN_POINT('Ctrl Pts',(47.0922739303984,-0.324015057350487,
329.092128572395));
#16473=CARTESIAN_POINT('Ctrl Pts',(47.0848768019349,-0.481405851956453,
329.100760613218));
#16474=CARTESIAN_POINT('Ctrl Pts',(47.0774796734715,-0.638461022105863,
329.115687056235));
#16475=CARTESIAN_POINT('Ctrl Pts',(47.070082545008,-0.794642547225585,329.136854616792));
#16476=CARTESIAN_POINT('Ctrl Pts',(47.0626842775714,-0.95084812040125,329.158025436624));
#16477=CARTESIAN_POINT('Ctrl Pts',(47.0552860101348,-1.10617941084858,329.1854392373));
#16478=CARTESIAN_POINT('Ctrl Pts',(47.0478877426982,-1.26010620016897,329.218991184335));
#16479=CARTESIAN_POINT('Ctrl Pts',(47.0404868761725,-1.41408706558918,329.252554918522));
#16480=CARTESIAN_POINT('Ctrl Pts',(47.0330860096467,-1.56666208307261,329.292261013015));
#16481=CARTESIAN_POINT('Ctrl Pts',(47.0256851431209,-1.7173140017749,329.337954152269));
#16482=CARTESIAN_POINT('Ctrl Pts',(47.0182761497362,-1.86813135068703,329.383697466958));
#16483=CARTESIAN_POINT('Ctrl Pts',(47.0108671563515,-2.01702102618953,329.435440847344));
#16484=CARTESIAN_POINT('Ctrl Pts',(47.0034581629667,-2.16348295330334,329.492979746427));
#16485=CARTESIAN_POINT('Ctrl Pts',(46.9960446053865,-2.31003510601626,329.550554091456));
#16486=CARTESIAN_POINT('Ctrl Pts',(46.9886310478062,-2.45415618936657,329.613930919474));
#16487=CARTESIAN_POINT('Ctrl Pts',(46.981217490226,-2.59536918869862,329.682858913208));
#16488=CARTESIAN_POINT('Ctrl Pts',(46.9737933780893,-2.73678323058761,329.751885038559));
#16489=CARTESIAN_POINT('Ctrl Pts',(46.9663692659526,-2.87528059197245,329.826477937205));
#16490=CARTESIAN_POINT('Ctrl Pts',(46.9589451538159,-3.01041107362125,329.906341616253));
#16491=CARTESIAN_POINT('Ctrl Pts',(46.9550880286612,-3.08061679928056,329.947834012883));
#16492=CARTESIAN_POINT('Ctrl Pts',(46.9512309035065,-3.14991423252374,329.990748412904));
#16493=CARTESIAN_POINT('Ctrl Pts',(46.9473737783518,-3.21824371641076,330.035038978574));
#16494=CARTESIAN_POINT('Ctrl Pts',(46.9399541975366,-3.349682574999,330.120236481418));
#16495=CARTESIAN_POINT('Ctrl Pts',(46.9325346167214,-3.4779353625985,330.210786306678));
#16496=CARTESIAN_POINT('Ctrl Pts',(46.9251150359061,-3.60253581249218,330.306422869259));
#16497=CARTESIAN_POINT('Ctrl Pts',(46.9177042145106,-3.72698916140179,330.401946525086));
#16498=CARTESIAN_POINT('Ctrl Pts',(46.9102933931151,-3.84779846173344,330.502544739512));
#16499=CARTESIAN_POINT('Ctrl Pts',(46.9028825717195,-3.96452442672832,330.607907488181));
#16500=CARTESIAN_POINT('Ctrl Pts',(46.8954788788627,-4.08113811192175,330.713168887434));
#16501=CARTESIAN_POINT('Ctrl Pts',(46.8880751860059,-4.19367600557905,330.823185448392));
#16502=CARTESIAN_POINT('Ctrl Pts',(46.880671493149,-4.30173016544464,330.937605614148));
#16503=CARTESIAN_POINT('Ctrl Pts',(46.8732733035934,-4.40970400666335,331.051940729288));
#16504=CARTESIAN_POINT('Ctrl Pts',(46.8658751140378,-4.51320049464683,331.170672661232));
#16505=CARTESIAN_POINT('Ctrl Pts',(46.8584769244822,-4.61184707517202,331.293411660607));
#16506=CARTESIAN_POINT('Ctrl Pts',(46.8510826173692,-4.7104418876698,331.416086248667));
#16507=CARTESIAN_POINT('Ctrl Pts',(46.8436883102561,-4.80419162790907,331.542763425736));
#16508=CARTESIAN_POINT('Ctrl Pts',(46.836294003143,-4.89276280918619,331.673018987799));
#16509=CARTESIAN_POINT('Ctrl Pts',(46.8289008955166,-4.98131962266,331.80325342012));
#16510=CARTESIAN_POINT('Ctrl Pts',(46.8215077878902,-5.06469933431005,331.937064776745));
#16511=CARTESIAN_POINT('Ctrl Pts',(46.8141146802638,-5.14261067861065,332.073998296183));
#16512=CARTESIAN_POINT('Ctrl Pts',(46.8067218718188,-5.22051887002503,332.210926274248));
#16513=CARTESIAN_POINT('Ctrl Pts',(46.7993290633738,-5.29295894924627,332.350975839106));
#16514=CARTESIAN_POINT('Ctrl Pts',(46.7919362549288,-5.35968482578323,332.493666197258));
#16515=CARTESIAN_POINT('Ctrl Pts',(46.7845422820638,-5.42642121212097,332.636379030158));
#16516=CARTESIAN_POINT('Ctrl Pts',(46.7771483091989,-5.48744144545509,332.781733145974));
#16517=CARTESIAN_POINT('Ctrl Pts',(46.7697543363339,-5.54254701029076,332.929226424445));
#16518=CARTESIAN_POINT('Ctrl Pts',(46.7623577350253,-5.59767216430661,333.076772134507));
#16519=CARTESIAN_POINT('Ctrl Pts',(46.7549611337168,-5.64687833301567,333.226458171368));
#16520=CARTESIAN_POINT('Ctrl Pts',(46.7475645324083,-5.69001647333298,333.377766016969));
#16521=CARTESIAN_POINT('Ctrl Pts',(46.7401598047119,-5.73320200802044,333.529240099224));
#16522=CARTESIAN_POINT('Ctrl Pts',(46.7327550770155,-5.77030609846415,333.68233918891));
#16523=CARTESIAN_POINT('Ctrl Pts',(46.7253503493191,-5.80123040153664,333.836532600033));
#16524=CARTESIAN_POINT('Ctrl Pts',(46.717941023626,-5.83217390718474,333.9908217582));
#16525=CARTESIAN_POINT('Ctrl Pts',(46.7105316979329,-5.85692992065084,334.146206223648));
#16526=CARTESIAN_POINT('Ctrl Pts',(46.7031223722398,-5.87545190896669,334.302149422928));
#16527=CARTESIAN_POINT('Ctrl Pts',(46.6957025664195,-5.89400009572497,334.458313196202));
#16528=CARTESIAN_POINT('Ctrl Pts',(46.6882827605993,-5.90629661854936,334.615036910139));
#16529=CARTESIAN_POINT('Ctrl Pts',(46.6808629547791,-5.91234702142441,334.77178242672));
#16530=CARTESIAN_POINT('Ctrl Pts',(46.677259304754,-5.91528558006071,334.847910562476));
#16531=CARTESIAN_POINT('Ctrl Pts',(46.6736556547288,-5.91675155731,334.924043887191));
#16532=CARTESIAN_POINT('Ctrl Pts',(46.6700520047037,-5.91674999875839,335.000121212992));
#16533=CARTESIAN_POINT('',(44.9200520047037,-5.91362697320443,334.994759399896));
#16534=CARTESIAN_POINT('Ctrl Pts',(46.6700520047037,-5.92649690913588,335.000121412671));
#16535=CARTESIAN_POINT('Ctrl Pts',(46.6697465844951,-5.92649885470028,335.006579817236));
#16536=CARTESIAN_POINT('Ctrl Pts',(46.6694411642864,-5.92648921301328,335.013038215818));
#16537=CARTESIAN_POINT('Ctrl Pts',(46.5763897326532,-5.92001614787365,336.980686933046));
#16538=CARTESIAN_POINT('Ctrl Pts',(46.3908977098039,-3.76689395428887,340.89602687056));
#16539=CARTESIAN_POINT('Ctrl Pts',(46.11265967553,2.91961231867273,341.358339942929));
#16540=CARTESIAN_POINT('Ctrl Pts',(45.8344216412561,6.92683346019826,335.985698298619));
#16541=CARTESIAN_POINT('Ctrl Pts',(45.556183606982,4.57740177519211,329.708495874547));
#16542=CARTESIAN_POINT('Ctrl Pts',(45.2779455727082,-1.972643956568,328.287228683932));
#16543=CARTESIAN_POINT('Ctrl Pts',(45.065901705282,-5.5848071039122,331.898755083066));
#16544=CARTESIAN_POINT('Ctrl Pts',(44.9466038492806,-5.91842218040601,334.430123096533));
#16545=CARTESIAN_POINT('Ctrl Pts',(44.9200520047037,-5.91362697320443,334.994759399896));
#16546=CARTESIAN_POINT('',(43.1700520047037,-5.90788815228446,335.002395865961));
#16547=CARTESIAN_POINT('Ctrl Pts',(44.9200520047037,-5.91362697320443,334.994759399896));
#16548=CARTESIAN_POINT('Ctrl Pts',(44.8538578378559,-5.90167244610358,336.402406599885));
#16549=CARTESIAN_POINT('Ctrl Pts',(44.6949176595833,-4.69332639461075,339.800777237329));
#16550=CARTESIAN_POINT('Ctrl Pts',(44.4432314698865,0.984477120973444,341.927007125697));
#16551=CARTESIAN_POINT('Ctrl Pts',(44.1649934356125,6.35782513266129,337.920733213378));
#16552=CARTESIAN_POINT('Ctrl Pts',(43.8867554013384,5.89669086145038,331.234145541087));
#16553=CARTESIAN_POINT('Ctrl Pts',(43.6085173670646,0.0242504217003248,
328.003426921824));
#16554=CARTESIAN_POINT('Ctrl Pts',(43.3696162348529,-5.03706062467533,330.742371873038));
#16555=CARTESIAN_POINT('Ctrl Pts',(43.223461114066,-5.90374971504265,333.863851207851));
#16556=CARTESIAN_POINT('Ctrl Pts',(43.1700520047037,-5.90788815228446,335.002395865961));
#16557=CARTESIAN_POINT('',(41.4200520047037,-5.92242663459137,335.004249368818));
#16558=CARTESIAN_POINT('Ctrl Pts',(43.1700520047037,-5.90788815228446,335.002395865961));
#16559=CARTESIAN_POINT('Ctrl Pts',(43.1307151026414,-5.91093619600615,335.840957306968));
#16560=CARTESIAN_POINT('Ctrl Pts',(42.9986321891541,-5.35183494074253,338.652745309149));
#16561=CARTESIAN_POINT('Ctrl Pts',(42.773803264243,-1.03247149672339,341.920016295474));
#16562=CARTESIAN_POINT('Ctrl Pts',(42.4955652299687,5.2604597648615,339.613045196343));
#16563=CARTESIAN_POINT('Ctrl Pts',(42.2173271956949,6.72594474449119,333.072750608958));
#16564=CARTESIAN_POINT('Ctrl Pts',(41.939089161421,2.01912950688338,328.30106434158));
#16565=CARTESIAN_POINT('Ctrl Pts',(41.6733307644238,-4.24639111760399,329.615183290383));
#16566=CARTESIAN_POINT('Ctrl Pts',(41.5003183788515,-5.90864287789061,333.303856397318));
#16567=CARTESIAN_POINT('Ctrl Pts',(41.4200520047037,-5.92242663459137,335.004249368818));
#16568=CARTESIAN_POINT('',(39.6700520047037,-5.92132355008389,334.995338312928));
#16569=CARTESIAN_POINT('Ctrl Pts',(41.4200520047037,-5.92242663459137,335.004249368818));
#16570=CARTESIAN_POINT('Ctrl Pts',(41.4075723674268,-5.92456970241727,335.268622685015));
#16571=CARTESIAN_POINT('Ctrl Pts',(41.3023467187248,-5.78826462712125,337.495538792487));
#16572=CARTESIAN_POINT('Ctrl Pts',(41.1043750585995,-2.96361819744428,341.337948414188));
#16573=CARTESIAN_POINT('Ctrl Pts',(40.826137024325,3.72593217667956,340.92199732658));
#16574=CARTESIAN_POINT('Ctrl Pts',(40.5478989900514,6.99624958693683,335.071516700898));
#16575=CARTESIAN_POINT('Ctrl Pts',(40.2696609557772,3.84621201573579,329.155406254391));
#16576=CARTESIAN_POINT('Ctrl Pts',(39.9914229215034,-2.83343755231025,328.602793222165));
#16577=CARTESIAN_POINT('Ctrl Pts',(39.7915532711454,-5.76386867538184,332.422934646081));
#16578=CARTESIAN_POINT('Ctrl Pts',(39.6844296322123,-5.92395602760576,334.690609525211));
#16579=CARTESIAN_POINT('Ctrl Pts',(39.6700520047037,-5.92132355008389,334.995338312928));
#16580=CARTESIAN_POINT('',(37.9200520047037,-5.90746150631063,334.998222585503));
#16581=CARTESIAN_POINT('Ctrl Pts',(39.6700520047037,-5.92132355008389,334.995338312928));
#16582=CARTESIAN_POINT('Ctrl Pts',(39.5916836207876,-5.90697465914474,336.656328807495));
#16583=CARTESIAN_POINT('Ctrl Pts',(39.4205692254472,-4.31103524867919,340.307183998279));
#16584=CARTESIAN_POINT('Ctrl Pts',(39.1567088186815,1.88176686553378,341.738811199685));
#16585=CARTESIAN_POINT('Ctrl Pts',(38.8784707844076,6.685142130748,337.064339510092));
#16586=CARTESIAN_POINT('Ctrl Pts',(38.6002327501337,5.35366113510944,330.495453921688));
#16587=CARTESIAN_POINT('Ctrl Pts',(38.3219947158598,-0.890795664309563,
328.060323782362));
#16588=CARTESIAN_POINT('Ctrl Pts',(38.0952678007163,-5.31306658525543,331.265445823351));
#16589=CARTESIAN_POINT('Ctrl Pts',(37.9612868969977,-5.90982214709327,334.11904235838));
#16590=CARTESIAN_POINT('Ctrl Pts',(37.9200520047037,-5.90746150631063,334.998222585503));
#16591=CARTESIAN_POINT('',(36.1700520047038,-5.9147878109749,335.005387872254));
#16592=CARTESIAN_POINT('Ctrl Pts',(37.9200520047037,-5.90746150631063,334.998222585503));
#16593=CARTESIAN_POINT('Ctrl Pts',(37.8685408855731,-5.90451256569713,336.096505008402));
#16594=CARTESIAN_POINT('Ctrl Pts',(37.724283755018,-5.08328597131374,339.176347489048));
#16595=CARTESIAN_POINT('Ctrl Pts',(37.4872806130378,-0.118779716061436,
341.99560678571));
#16596=CARTESIAN_POINT('Ctrl Pts',(37.209042578764,5.81847647089011,338.885608636871));
#16597=CARTESIAN_POINT('Ctrl Pts',(36.9308045444899,6.4162026810768,332.209844793464));
#16598=CARTESIAN_POINT('Ctrl Pts',(36.6525665102162,1.12587439383617,328.094565200472));
#16599=CARTESIAN_POINT('Ctrl Pts',(36.3989823302873,-4.63734310247643,330.119439702854));
#16600=CARTESIAN_POINT('Ctrl Pts',(36.2381441617832,-5.90195021880725,333.558100165989));
#16601=CARTESIAN_POINT('Ctrl Pts',(36.1700520047038,-5.9147878109749,335.005387872254));
#16602=CARTESIAN_POINT('',(34.4200520047038,-5.92198531706792,334.999129254866));
#16603=CARTESIAN_POINT('Ctrl Pts',(36.1700520047038,-5.9147878109749,335.005387872254));
#16604=CARTESIAN_POINT('Ctrl Pts',(36.1453981503586,-5.91943586650756,335.529401530159));
#16605=CARTESIAN_POINT('Ctrl Pts',(36.027998284589,-5.6153715872659,338.019412061154));
#16606=CARTESIAN_POINT('Ctrl Pts',(35.8178524073941,-2.10945529650313,341.671043492088));
#16607=CARTESIAN_POINT('Ctrl Pts',(35.5396143731204,4.46827549150828,340.383970380044));
#16608=CARTESIAN_POINT('Ctrl Pts',(35.2613763388463,6.94553581259915,334.156107117514));
#16609=CARTESIAN_POINT('Ctrl Pts',(34.9831383045725,3.04898043440978,328.702671897399));
#16610=CARTESIAN_POINT('Ctrl Pts',(34.7049002702983,-3.64557928556341,329.028201728633));
#16611=CARTESIAN_POINT('Ctrl Pts',(34.517204837009,-5.90481133641296,332.944685763767));
#16612=CARTESIAN_POINT('Ctrl Pts',(34.4222554151441,-5.92643859533875,334.952532118383));
#16613=CARTESIAN_POINT('Ctrl Pts',(34.4200520047038,-5.92634295523124,334.999128614136));
#16614=CARTESIAN_POINT('',(32.6700520280108,-5.91402521091767,334.995077176078));
#16615=CARTESIAN_POINT('Ctrl Pts',(34.4200520047038,-5.91674993604115,334.999130024655));
#16616=CARTESIAN_POINT('Ctrl Pts',(34.4126579298141,-5.91677289021799,335.155242637744));
#16617=CARTESIAN_POINT('Ctrl Pts',(34.4052638549244,-5.91061306742824,335.311599720021));
#16618=CARTESIAN_POINT('Ctrl Pts',(34.3978697800347,-5.89823842825458,335.467668692517));
#16619=CARTESIAN_POINT('Ctrl Pts',(34.3904843951807,-5.88587833262526,335.623554241805));
#16620=CARTESIAN_POINT('Ctrl Pts',(34.3830990103266,-5.86731798692203,335.779151983579));
#16621=CARTESIAN_POINT('Ctrl Pts',(34.3757136254726,-5.84257731564632,335.933927659509));
#16622=CARTESIAN_POINT('Ctrl Pts',(34.3683352764739,-5.81786021413507,336.088555884862));
#16623=CARTESIAN_POINT('Ctrl Pts',(34.3609569274751,-5.7869745660705,336.242363233957));
#16624=CARTESIAN_POINT('Ctrl Pts',(34.3535785784763,-5.74999220681904,336.394819050637));
#16625=CARTESIAN_POINT('Ctrl Pts',(34.3462056169747,-5.71303685121784,336.54716354766));
#16626=CARTESIAN_POINT('Ctrl Pts',(34.338832655473,-5.66999373564674,336.698158112603));
#16627=CARTESIAN_POINT('Ctrl Pts',(34.3314596939714,-5.62098600697052,336.847280940177));
#16628=CARTESIAN_POINT('Ctrl Pts',(34.3238332151289,-5.57029316044088,337.001531316933));
#16629=CARTESIAN_POINT('Ctrl Pts',(34.3162067362864,-5.5132182511541,337.153778529582));
#16630=CARTESIAN_POINT('Ctrl Pts',(34.3085802574439,-5.44995434787204,337.303460042764));
#16631=CARTESIAN_POINT('Ctrl Pts',(34.3012120822682,-5.38883315009494,337.448071944594));
#16632=CARTESIAN_POINT('Ctrl Pts',(34.2938439070925,-5.3219355205658,337.590288740651));
#16633=CARTESIAN_POINT('Ctrl Pts',(34.2864757319169,-5.24948504540392,337.729622193744));
#16634=CARTESIAN_POINT('Ctrl Pts',(34.2791076357912,-5.17703534753248,337.868954151988));
#16635=CARTESIAN_POINT('Ctrl Pts',(34.2717395396656,-5.09903309590665,338.005402494501));
#16636=CARTESIAN_POINT('Ctrl Pts',(34.26437144354,-5.0157481858264,338.138502939122));
#16637=CARTESIAN_POINT('Ctrl Pts',(34.2570019419513,-4.93244738916414,338.27162877263));
#16638=CARTESIAN_POINT('Ctrl Pts',(34.2496324403626,-4.84386212789593,338.401405117803));
#16639=CARTESIAN_POINT('Ctrl Pts',(34.2422629387739,-4.75030591952179,338.527396239928));
#16640=CARTESIAN_POINT('Ctrl Pts',(34.2348905465991,-4.65671301500481,338.653436780347));
#16641=CARTESIAN_POINT('Ctrl Pts',(34.2275181544243,-4.55814550637757,338.775688840202));
#16642=CARTESIAN_POINT('Ctrl Pts',(34.2201457622494,-4.45495738023128,338.893749517216));
#16643=CARTESIAN_POINT('Ctrl Pts',(34.2127652038723,-4.3516549553489,339.011940966895));
#16644=CARTESIAN_POINT('Ctrl Pts',(34.2053846454953,-4.24372194256433,339.125931481295));
#16645=CARTESIAN_POINT('Ctrl Pts',(34.1980040871182,-4.13154982505284,339.235354366001));
#16646=CARTESIAN_POINT('Ctrl Pts',(34.1906186555257,-4.01930364283438,339.344849500158));
#16647=CARTESIAN_POINT('Ctrl Pts',(34.1832332239331,-3.90281305889682,339.449770745627));
#16648=CARTESIAN_POINT('Ctrl Pts',(34.1758477923406,-3.78250235883659,339.549791914791));
#16649=CARTESIAN_POINT('Ctrl Pts',(34.1684523991843,-3.66202938217995,339.649947993775));
#16650=CARTESIAN_POINT('Ctrl Pts',(34.1610570060282,-3.53772630150714,339.745190575623));
#16651=CARTESIAN_POINT('Ctrl Pts',(34.1536616128719,-3.41004651512151,339.835236636113));
#16652=CARTESIAN_POINT('Ctrl Pts',(34.1519158091648,-3.37990560987346,339.856493483841));
#16653=CARTESIAN_POINT('Ctrl Pts',(34.1501700054577,-3.34957663745125,339.877460945083));
#16654=CARTESIAN_POINT('Ctrl Pts',(34.1484242017506,-3.31906575364121,339.898135674469));
#16655=CARTESIAN_POINT('Ctrl Pts',(34.1410002243126,-3.18931914347101,339.986054335586));
#16656=CARTESIAN_POINT('Ctrl Pts',(34.1335762468746,-3.05588107845703,340.068946783448));
#16657=CARTESIAN_POINT('Ctrl Pts',(34.1261522694366,-2.91917841302769,340.146486952807));
#16658=CARTESIAN_POINT('Ctrl Pts',(34.118737053409,-2.78263707731139,340.2239356131));
#16659=CARTESIAN_POINT('Ctrl Pts',(34.1113218373814,-2.64283913154804,340.296044385628));
#16660=CARTESIAN_POINT('Ctrl Pts',(34.1039066213538,-2.50024182317893,340.362529383428));
#16661=CARTESIAN_POINT('Ctrl Pts',(34.0964985402097,-2.35778172122227,340.428950409697));
#16662=CARTESIAN_POINT('Ctrl Pts',(34.0890904590657,-2.21252795497314,340.48975827721));
#16663=CARTESIAN_POINT('Ctrl Pts',(34.0816823779216,-2.06496379158148,340.544714158724));
#16664=CARTESIAN_POINT('Ctrl Pts',(34.0742798107476,-1.91750946289127,340.599629135573));
#16665=CARTESIAN_POINT('Ctrl Pts',(34.0668772435735,-1.76774850941976,340.648700669642));
#16666=CARTESIAN_POINT('Ctrl Pts',(34.0594746763995,-1.61618557159137,340.691737411431));
#16667=CARTESIAN_POINT('Ctrl Pts',(34.0520760066447,-1.46470243098648,340.734751494563));
#16668=CARTESIAN_POINT('Ctrl Pts',(34.0446773368899,-1.31141955360445,340.771737011493));
#16669=CARTESIAN_POINT('Ctrl Pts',(34.0372786671352,-1.156858082969,340.802552019445));
#16670=CARTESIAN_POINT('Ctrl Pts',(34.0298812179312,-1.00232211017793,340.833361943877));
#16671=CARTESIAN_POINT('Ctrl Pts',(34.0224837687272,-0.84650832840989,340.858003306718));
#16672=CARTESIAN_POINT('Ctrl Pts',(34.0150863195233,-0.689949572475246,
340.876384955901));
#16673=CARTESIAN_POINT('Ctrl Pts',(34.0076891910598,-0.533397604655317,
340.894765808088));
#16674=CARTESIAN_POINT('Ctrl Pts',(34.0002920625963,-0.376101097558557,
340.90688744275));
#16675=CARTESIAN_POINT('Ctrl Pts',(33.9928949341329,-0.218599266019462,
340.912710454893));
#16676=CARTESIAN_POINT('Ctrl Pts',(33.9854966666963,-0.0610731831300849,
340.918534363633));
#16677=CARTESIAN_POINT('Ctrl Pts',(33.9780983992597,0.0966579141717653,
340.918057705003));
#16678=CARTESIAN_POINT('Ctrl Pts',(33.9707001318231,0.254053692634734,340.911293198934));
#16679=CARTESIAN_POINT('Ctrl Pts',(33.9632992652973,0.411504765890113,340.904526316422));
#16680=CARTESIAN_POINT('Ctrl Pts',(33.9558983987716,0.568619913132773,340.891467204396));
#16681=CARTESIAN_POINT('Ctrl Pts',(33.9484975322458,0.724862954722387,340.872180537021));
#16682=CARTESIAN_POINT('Ctrl Pts',(33.9410885388611,0.881277566109089,340.852872691042));
#16683=CARTESIAN_POINT('Ctrl Pts',(33.9336795454763,1.03681778873289,340.827323678711));
#16684=CARTESIAN_POINT('Ctrl Pts',(33.9262705520916,1.19095595648239,340.795649616067));
#16685=CARTESIAN_POINT('Ctrl Pts',(33.9188569945113,1.34518907866002,340.763956041108));
#16686=CARTESIAN_POINT('Ctrl Pts',(33.9114434369311,1.4980180634654,340.726129986608));
#16687=CARTESIAN_POINT('Ctrl Pts',(33.9040298793509,1.64892997670942,340.682337590676));
#16688=CARTESIAN_POINT('Ctrl Pts',(33.8966057672142,1.80005674068985,340.638482848251));
#16689=CARTESIAN_POINT('Ctrl Pts',(33.8891816550775,1.94926062911523,340.58864491774));
#16690=CARTESIAN_POINT('Ctrl Pts',(33.8817575429408,2.0960474974414,340.533038536913));
#16691=CARTESIAN_POINT('Ctrl Pts',(33.8779004177861,2.17230918527429,340.504148783324));
#16692=CARTESIAN_POINT('Ctrl Pts',(33.8740432926314,2.24791884239155,340.47370276989));
#16693=CARTESIAN_POINT('Ctrl Pts',(33.8701861674767,2.32280985855492,340.44173546982));
#16694=CARTESIAN_POINT('Ctrl Pts',(33.8627621900387,2.46695587197247,340.380206609607));
#16695=CARTESIAN_POINT('Ctrl Pts',(33.8553382126007,2.60887289346655,340.312853553867));
#16696=CARTESIAN_POINT('Ctrl Pts',(33.8479142351627,2.7480557323888,340.239858800978));
#16697=CARTESIAN_POINT('Ctrl Pts',(33.8404990191351,2.88707431461993,340.16695019288));
#16698=CARTESIAN_POINT('Ctrl Pts',(33.8330838031074,3.02336480986931,340.088413312245));
#16699=CARTESIAN_POINT('Ctrl Pts',(33.8256685870798,3.15644104870449,340.004479040675));
#16700=CARTESIAN_POINT('Ctrl Pts',(33.8182605059357,3.2893892422528,339.920625530238));
#16701=CARTESIAN_POINT('Ctrl Pts',(33.8108524247916,3.41912902290022,339.831385165612));
#16702=CARTESIAN_POINT('Ctrl Pts',(33.8034443436475,3.54519803213956,339.737035093327));
#16703=CARTESIAN_POINT('Ctrl Pts',(33.7960417764735,3.67117320591284,339.642755247525));
#16704=CARTESIAN_POINT('Ctrl Pts',(33.7886392092995,3.79348275101191,339.54337348955));
#16705=CARTESIAN_POINT('Ctrl Pts',(33.7812366421255,3.91169266766929,339.439210632106));
#16706=CARTESIAN_POINT('Ctrl Pts',(33.7738379723707,4.02984034732235,339.335102615951));
#16707=CARTESIAN_POINT('Ctrl Pts',(33.766439302616,4.14389241788081,339.226218759654));
#16708=CARTESIAN_POINT('Ctrl Pts',(33.7590406328613,4.25344749597255,339.11292049054));
#16709=CARTESIAN_POINT('Ctrl Pts',(33.7516431836573,4.36298450087812,338.999640912123));
#16710=CARTESIAN_POINT('Ctrl Pts',(33.7442457344533,4.46802572649885,338.881948634247));
#16711=CARTESIAN_POINT('Ctrl Pts',(33.7368482852493,4.56820617362811,338.760242401458));
#16712=CARTESIAN_POINT('Ctrl Pts',(33.7294511567858,4.66838227710783,338.63854144564));
#16713=CARTESIAN_POINT('Ctrl Pts',(33.7220540283224,4.76369778396113,338.512827169104));
#16714=CARTESIAN_POINT('Ctrl Pts',(33.7146568998589,4.85382775759897,338.383531684802));
#16715=CARTESIAN_POINT('Ctrl Pts',(33.7072586324223,4.94397160900281,338.254216292224));
#16716=CARTESIAN_POINT('Ctrl Pts',(33.6998603649857,5.02892812395047,338.121318900122));
#16717=CARTESIAN_POINT('Ctrl Pts',(33.6924620975491,5.10841559357635,337.985300769739));
#16718=CARTESIAN_POINT('Ctrl Pts',(33.6850612310234,5.1879309879861,337.849234854757));
#16719=CARTESIAN_POINT('Ctrl Pts',(33.6776603644977,5.26197332351767,337.710046340687));
#16720=CARTESIAN_POINT('Ctrl Pts',(33.6702594979719,5.33030682848717,337.56822111133));
#16721=CARTESIAN_POINT('Ctrl Pts',(33.6628505045872,5.39871537017816,337.426240144313));
#16722=CARTESIAN_POINT('Ctrl Pts',(33.6554415112023,5.46140240000281,337.281617016229));
#16723=CARTESIAN_POINT('Ctrl Pts',(33.6480325178176,5.51818001200433,337.134858289821));
#16724=CARTESIAN_POINT('Ctrl Pts',(33.6406189602374,5.57499260097331,336.988009154975));
#16725=CARTESIAN_POINT('Ctrl Pts',(33.6332054026572,5.62588839776436,336.83902215264));
#16726=CARTESIAN_POINT('Ctrl Pts',(33.6257918450769,5.67072953333535,336.688418526983));
#16727=CARTESIAN_POINT('Ctrl Pts',(33.6183677329402,5.71563450847209,336.537600489492));
#16728=CARTESIAN_POINT('Ctrl Pts',(33.6109436208036,5.75446751480416,336.385161592691));
#16729=CARTESIAN_POINT('Ctrl Pts',(33.6035195086669,5.78714171993692,336.231633580196));
#16730=CARTESIAN_POINT('Ctrl Pts',(33.5996623835122,5.80411728498861,336.151869596565));
#16731=CARTESIAN_POINT('Ctrl Pts',(33.5958052583575,5.81943130670169,336.071811737973));
#16732=CARTESIAN_POINT('Ctrl Pts',(33.5919481332028,5.8330771481725,335.991534944401));
#16733=CARTESIAN_POINT('Ctrl Pts',(33.5845241557648,5.85934189591565,335.837022689711));
#16734=CARTESIAN_POINT('Ctrl Pts',(33.5771001783268,5.87950271795634,335.681233035491));
#16735=CARTESIAN_POINT('Ctrl Pts',(33.5696762008888,5.89343969342769,335.524689567679));
#16736=CARTESIAN_POINT('Ctrl Pts',(33.5622609848611,5.90736022117104,335.368330844712));
#16737=CARTESIAN_POINT('Ctrl Pts',(33.5548457688335,5.91507149006048,335.21122044707));
#16738=CARTESIAN_POINT('Ctrl Pts',(33.5474305528058,5.91650455918472,335.053892148282));
#16739=CARTESIAN_POINT('Ctrl Pts',(33.5400224716617,5.91793624941707,334.896715229991));
#16740=CARTESIAN_POINT('Ctrl Pts',(33.5326143905177,5.9131017627182,334.739321198657));
#16741=CARTESIAN_POINT('Ctrl Pts',(33.5252063093735,5.90198394880129,334.582248841304));
#16742=CARTESIAN_POINT('Ctrl Pts',(33.5178037421995,5.89087441007637,334.425293395776));
#16743=CARTESIAN_POINT('Ctrl Pts',(33.5104011750255,5.87349088255147,334.268659518178));
#16744=CARTESIAN_POINT('Ctrl Pts',(33.5029986078515,5.84986828229686,334.112885778337));
#16745=CARTESIAN_POINT('Ctrl Pts',(33.4955999380967,5.82625811923782,333.957194052687));
#16746=CARTESIAN_POINT('Ctrl Pts',(33.4882012683419,5.79641548122736,333.802361930962));
#16747=CARTESIAN_POINT('Ctrl Pts',(33.4808025985871,5.76042708864121,333.648922534068));
#16748=CARTESIAN_POINT('Ctrl Pts',(33.4734051493831,5.7244446330226,333.495508449911));
#16749=CARTESIAN_POINT('Ctrl Pts',(33.4660077001791,5.68231852014944,333.34348699759));
#16750=CARTESIAN_POINT('Ctrl Pts',(33.4586102509751,5.63418654080336,333.193380896279));
#16751=CARTESIAN_POINT('Ctrl Pts',(33.4512131225117,5.58605664837599,333.043281303306));
#16752=CARTESIAN_POINT('Ctrl Pts',(33.4438159940482,5.5319215212007,332.895097251609));
#16753=CARTESIAN_POINT('Ctrl Pts',(33.4364188655847,5.47196869044563,332.749335828409));
#16754=CARTESIAN_POINT('Ctrl Pts',(33.4290205981481,5.41200662845135,332.603551961589));
#16755=CARTESIAN_POINT('Ctrl Pts',(33.4216223307115,5.34622522123311,332.460191811185));
#16756=CARTESIAN_POINT('Ctrl Pts',(33.4142240632749,5.27485990437902,332.319741887117));
#16757=CARTESIAN_POINT('Ctrl Pts',(33.4068231967491,5.20346951613872,332.179242621514));
#16758=CARTESIAN_POINT('Ctrl Pts',(33.3994223302234,5.12649148150508,332.041655950343));
#16759=CARTESIAN_POINT('Ctrl Pts',(33.3920214636977,5.04420680094495,331.907443078648));
#16760=CARTESIAN_POINT('Ctrl Pts',(33.3846124703129,4.96183176393849,331.773082828388));
#16761=CARTESIAN_POINT('Ctrl Pts',(33.3772034769281,4.87413863895259,331.64210409456));
#16762=CARTESIAN_POINT('Ctrl Pts',(33.3697944835434,4.78145171870812,331.514939021457));
#16763=CARTESIAN_POINT('Ctrl Pts',(33.3623809259632,4.68870770012433,331.387695610284));
#16764=CARTESIAN_POINT('Ctrl Pts',(33.354967368383,4.59096398740696,331.264270833113));
#16765=CARTESIAN_POINT('Ctrl Pts',(33.3475538108028,4.48858429704586,331.145062702091));
#16766=CARTESIAN_POINT('Ctrl Pts',(33.3401296986661,4.38605885045184,331.025684856469));
#16767=CARTESIAN_POINT('Ctrl Pts',(33.3327055865294,4.27888449795346,330.910535918977));
#16768=CARTESIAN_POINT('Ctrl Pts',(33.3252814743927,4.1674614041125,330.799976665811));
#16769=CARTESIAN_POINT('Ctrl Pts',(33.3214243492381,4.10957262089594,330.742536682604));
#16770=CARTESIAN_POINT('Ctrl Pts',(33.3175672240835,4.05053755551535,330.686334894033));
#16771=CARTESIAN_POINT('Ctrl Pts',(33.3137100989289,3.9904156349902,330.631417435538));
#16772=CARTESIAN_POINT('Ctrl Pts',(33.3062861214909,3.87469634572208,330.525715401903));
#16773=CARTESIAN_POINT('Ctrl Pts',(33.2988621440529,3.75459967949589,330.424455015429));
#16774=CARTESIAN_POINT('Ctrl Pts',(33.2914381666149,3.63050103483573,330.328020462528));
#16775=CARTESIAN_POINT('Ctrl Pts',(33.2840229505872,3.50654884524791,330.231699716908));
#16776=CARTESIAN_POINT('Ctrl Pts',(33.2766077345596,3.37860437013577,330.14019369523));
#16777=CARTESIAN_POINT('Ctrl Pts',(33.269192518532,3.24707916316589,330.05384922686));
#16778=CARTESIAN_POINT('Ctrl Pts',(33.2617844373879,3.11568050908782,329.967587838703));
#16779=CARTESIAN_POINT('Ctrl Pts',(33.2543763562438,2.98070829212938,329.886478320085));
#16780=CARTESIAN_POINT('Ctrl Pts',(33.2469682750997,2.84260630878921,329.810826661622));
#16781=CARTESIAN_POINT('Ctrl Pts',(33.2395657079257,2.70460711727768,329.735231312071));
#16782=CARTESIAN_POINT('Ctrl Pts',(33.2321631407517,2.56348312375822,329.665085912409));
#16783=CARTESIAN_POINT('Ctrl Pts',(33.2247605735777,2.4197061181765,329.600652552006));
#16784=CARTESIAN_POINT('Ctrl Pts',(33.2173619038229,2.27600481055944,329.536253115485));
#16785=CARTESIAN_POINT('Ctrl Pts',(33.2099632340682,2.12965361240599,329.477559881123));
#16786=CARTESIAN_POINT('Ctrl Pts',(33.2025645643134,1.98114776583088,329.424788426217));
#16787=CARTESIAN_POINT('Ctrl Pts',(33.1951671151094,1.83266641810952,329.372025676963));
#16788=CARTESIAN_POINT('Ctrl Pts',(33.1877696659055,1.6820314787462,329.325182893159));
#16789=CARTESIAN_POINT('Ctrl Pts',(33.1803722167015,1.52975707994427,329.284427076936));
#16790=CARTESIAN_POINT('Ctrl Pts',(33.1729750882381,1.3774892834948,329.243673027814));
#16791=CARTESIAN_POINT('Ctrl Pts',(33.1655779597746,1.22358252946698,329.209005518005));
#16792=CARTESIAN_POINT('Ctrl Pts',(33.1581808313111,1.06856472220108,329.180541262543));
#16793=CARTESIAN_POINT('Ctrl Pts',(33.1507825638745,0.913523046062173,329.152072624295));
#16794=CARTESIAN_POINT('Ctrl Pts',(33.1433842964379,0.757370343150165,329.129809209622));
#16795=CARTESIAN_POINT('Ctrl Pts',(33.1359860290013,0.600643137742669,329.113816314149));
#16796=CARTESIAN_POINT('Ctrl Pts',(33.1285851624755,0.443860872419733,329.097817800203));
#16797=CARTESIAN_POINT('Ctrl Pts',(33.1211842959498,0.28650407380993,329.088094229288));
#16798=CARTESIAN_POINT('Ctrl Pts',(33.113783429424,0.129112644549985,329.084658886631));
#16799=CARTESIAN_POINT('Ctrl Pts',(33.1063744360392,-0.0284516155462758,
329.081219771638));
#16800=CARTESIAN_POINT('Ctrl Pts',(33.0989654426544,-0.186050208891175,
329.084082682857));
#16801=CARTESIAN_POINT('Ctrl Pts',(33.0915564492697,-0.343144242729558,
329.093208773693));
#16802=CARTESIAN_POINT('Ctrl Pts',(33.0841428916894,-0.500335051911762,
329.102340486515));
#16803=CARTESIAN_POINT('Ctrl Pts',(33.0767293341092,-0.657020311672226,
329.11774303077));
#16804=CARTESIAN_POINT('Ctrl Pts',(33.069315776529,-0.812668497243394,329.139325936713));
#16805=CARTESIAN_POINT('Ctrl Pts',(33.0618916643923,-0.968538276501934,
329.160939569873));
#16806=CARTESIAN_POINT('Ctrl Pts',(33.0544675522556,-1.12336766643381,329.188751072032));
#16807=CARTESIAN_POINT('Ctrl Pts',(33.0470434401189,-1.27663673063275,329.222619172973));
#16808=CARTESIAN_POINT('Ctrl Pts',(33.0431863149643,-1.35626618019799,329.240215014964));
#16809=CARTESIAN_POINT('Ctrl Pts',(33.0393291898095,-1.43547472452992,329.259444848248));
#16810=CARTESIAN_POINT('Ctrl Pts',(33.0354720646549,-1.51419140798456,329.280283665907));
#16811=CARTESIAN_POINT('Ctrl Pts',(33.0280480872168,-1.66570085051652,329.320393049435));
#16812=CARTESIAN_POINT('Ctrl Pts',(33.0206241097789,-1.81584406703773,329.366587092774));
#16813=CARTESIAN_POINT('Ctrl Pts',(33.0132001323409,-1.96409483731779,329.418758020609));
#16814=CARTESIAN_POINT('Ctrl Pts',(33.0057849163133,-2.11217064938319,329.470867378899));
#16815=CARTESIAN_POINT('Ctrl Pts',(32.9983697002856,-2.25835811214371,329.528939458651));
#16816=CARTESIAN_POINT('Ctrl Pts',(32.990954484258,-2.40214285408021,329.59281586488));
#16817=CARTESIAN_POINT('Ctrl Pts',(32.9835464031139,-2.54578924706228,329.656630809553));
#16818=CARTESIAN_POINT('Ctrl Pts',(32.9761383219698,-2.68703718296428,329.726238811711));
#16819=CARTESIAN_POINT('Ctrl Pts',(32.9687302408257,-2.82538918399848,329.801432262493));
#16820=CARTESIAN_POINT('Ctrl Pts',(32.9613276736517,-2.96363820711171,329.876569745417));
#16821=CARTESIAN_POINT('Ctrl Pts',(32.9539251064777,-3.09899526076012,329.957284221617));
#16822=CARTESIAN_POINT('Ctrl Pts',(32.9465225393037,-3.23098463579218,330.043320784459));
#16823=CARTESIAN_POINT('Ctrl Pts',(32.9391238695489,-3.36290451899495,330.129312049427));
#16824=CARTESIAN_POINT('Ctrl Pts',(32.9317251997942,-3.49145994288626,330.220619617289));
#16825=CARTESIAN_POINT('Ctrl Pts',(32.9243265300394,-3.61620161999129,330.316943689633));
#16826=CARTESIAN_POINT('Ctrl Pts',(32.9169290808355,-3.74092271859286,330.413251871495));
#16827=CARTESIAN_POINT('Ctrl Pts',(32.9095316316315,-3.86183102396098,330.514574687506));
#16828=CARTESIAN_POINT('Ctrl Pts',(32.9021341824276,-3.97850787400498,330.620570167364));
#16829=CARTESIAN_POINT('Ctrl Pts',(32.8947370539641,-4.09517966514451,330.726561051443));
#16830=CARTESIAN_POINT('Ctrl Pts',(32.8873399255006,-4.20762008951414,330.837223945583));
#16831=CARTESIAN_POINT('Ctrl Pts',(32.8799427970371,-4.3154453196227,330.952178084964));
#16832=CARTESIAN_POINT('Ctrl Pts',(32.8725445296005,-4.42328715212455,331.067149924412));
#16833=CARTESIAN_POINT('Ctrl Pts',(32.8651462621639,-4.52651212007774,331.186414052508));
#16834=CARTESIAN_POINT('Ctrl Pts',(32.8577479947274,-4.62477497092559,331.30955462975));
#16835=CARTESIAN_POINT('Ctrl Pts',(32.8503471282016,-4.72307234254658,331.432738467572));
#16836=CARTESIAN_POINT('Ctrl Pts',(32.8429462616758,-4.8164038936307,331.559801174423));
#16837=CARTESIAN_POINT('Ctrl Pts',(32.8355453951501,-4.90446628005209,331.690295924054));
#16838=CARTESIAN_POINT('Ctrl Pts',(32.8281364017653,-4.99262536739299,331.820933969397));
#16839=CARTESIAN_POINT('Ctrl Pts',(32.8207274083806,-5.0755035261362,331.955011274293));
#16840=CARTESIAN_POINT('Ctrl Pts',(32.8133184149958,-5.15284179741967,332.092053650209));
#16841=CARTESIAN_POINT('Ctrl Pts',(32.8059048574156,-5.23022771174594,332.229180448955));
#16842=CARTESIAN_POINT('Ctrl Pts',(32.7984912998354,-5.30206676833751,332.369275627115));
#16843=CARTESIAN_POINT('Ctrl Pts',(32.7910777422551,-5.36814740658304,332.511843255802));
#16844=CARTESIAN_POINT('Ctrl Pts',(32.7836536301184,-5.4343221227146,332.654613855609));
#16845=CARTESIAN_POINT('Ctrl Pts',(32.7762295179817,-5.49472190421748,332.799863592385));
#16846=CARTESIAN_POINT('Ctrl Pts',(32.7688054058451,-5.54918418080667,332.947078791092));
#16847=CARTESIAN_POINT('Ctrl Pts',(32.7649482806904,-5.57747952618227,333.023563013802));
#16848=CARTESIAN_POINT('Ctrl Pts',(32.7610911555357,-5.6041730374472,333.100577534769));
#16849=CARTESIAN_POINT('Ctrl Pts',(32.757234030381,-5.62924734528016,333.1780491532));
#16850=CARTESIAN_POINT('Ctrl Pts',(32.7483245768245,-5.68716570990079,333.35699843762));
#16851=CARTESIAN_POINT('Ctrl Pts',(32.7394151232681,-5.73658396790036,333.53882492236));
#16852=CARTESIAN_POINT('Ctrl Pts',(32.7305056697117,-5.77725438143087,333.722791178101));
#16853=CARTESIAN_POINT('Ctrl Pts',(32.7216448111127,-5.817702965755,333.905754024115));
#16854=CARTESIAN_POINT('Ctrl Pts',(32.7127839525136,-5.84949880810189,334.090833337918));
#16855=CARTESIAN_POINT('Ctrl Pts',(32.7039230939145,-5.8724449569823,334.277282358239));
#16856=CARTESIAN_POINT('Ctrl Pts',(32.6951516005632,-5.89515968491686,334.46185096678));
#16857=CARTESIAN_POINT('Ctrl Pts',(32.6863801072118,-5.90920226207405,334.64776174815));
#16858=CARTESIAN_POINT('Ctrl Pts',(32.6776086138604,-5.91442846696909,334.834269883227));
#16859=CARTESIAN_POINT('Ctrl Pts',(32.6750897633767,-5.91592924091947,334.887828164289));
#16860=CARTESIAN_POINT('Ctrl Pts',(32.672570912893,-5.91670329426,334.941435577252));
#16861=CARTESIAN_POINT('Ctrl Pts',(32.6700520624094,-5.9167479495726,334.995074177391));
#16862=CARTESIAN_POINT('',(30.9200520047038,-5.90864326687124,335.003157960057));
#16863=CARTESIAN_POINT('Ctrl Pts',(32.6700520047037,-5.91218039106208,334.99507920787));
#16864=CARTESIAN_POINT('Ctrl Pts',(32.6063666685048,-5.90157038152927,336.350213184948));
#16865=CARTESIAN_POINT('Ctrl Pts',(32.4499353208814,-4.76532520505771,339.694927843386));
#16866=CARTESIAN_POINT('Ctrl Pts',(32.200757961833,0.796951585255475,341.951078412161));
#16867=CARTESIAN_POINT('Ctrl Pts',(31.9225199275592,6.27658636339294,338.091453791354));
#16868=CARTESIAN_POINT('Ctrl Pts',(31.6442818932852,5.99629047810708,331.39484765601));
#16869=CARTESIAN_POINT('Ctrl Pts',(31.3660438590111,0.213287326162839,328.006636614779));
#16870=CARTESIAN_POINT('Ctrl Pts',(31.1246338961508,-4.97409082752309,330.63514264744));
#16871=CARTESIAN_POINT('Ctrl Pts',(30.975969944715,-5.90288956727121,333.811512346957));
#16872=CARTESIAN_POINT('Ctrl Pts',(30.9200520047038,-5.90864326687124,335.003157960057));
#16873=CARTESIAN_POINT('',(29.1700520047038,-5.92375170242329,335.003585402275));
#16874=CARTESIAN_POINT('Ctrl Pts',(30.9200520047038,-5.90864326687124,335.003157960057));
#16875=CARTESIAN_POINT('Ctrl Pts',(30.8832239332903,-5.91243270653441,335.787986759724));
#16876=CARTESIAN_POINT('Ctrl Pts',(30.7536498504522,-5.40138091405304,338.544554349899));
#16877=CARTESIAN_POINT('Ctrl Pts',(30.5313297561895,-1.2190717529215,341.889592657226));
#16878=CARTESIAN_POINT('Ctrl Pts',(30.2530917219154,5.13389577264302,339.753497356351));
#16879=CARTESIAN_POINT('Ctrl Pts',(29.9748536876416,6.77556292383056,333.255187693066));
#16880=CARTESIAN_POINT('Ctrl Pts',(29.6966156533676,2.19939598696192,328.35806653046));
#16881=CARTESIAN_POINT('Ctrl Pts',(29.4283484257217,-4.158806077555,329.513215736931));
#16882=CARTESIAN_POINT('Ctrl Pts',(29.2528272095004,-5.91124546303899,333.251071106676));
#16883=CARTESIAN_POINT('Ctrl Pts',(29.1700520047038,-5.92375170242329,335.003585402275));
#16884=CARTESIAN_POINT('',(27.4200520047038,-5.91977329940477,334.994921843694));
#16885=CARTESIAN_POINT('Ctrl Pts',(29.1700520047038,-5.92375170242329,335.003585402275));
#16886=CARTESIAN_POINT('Ctrl Pts',(29.1600811980758,-5.92525815951815,335.214687038293));
#16887=CARTESIAN_POINT('Ctrl Pts',(29.0573643800223,-5.81911313062826,337.387873149651));
#16888=CARTESIAN_POINT('Ctrl Pts',(28.8619015505466,-3.13378605384101,341.255558159747));
#16889=CARTESIAN_POINT('Ctrl Pts',(28.5836635162714,3.5645608626718,341.020509013158));
#16890=CARTESIAN_POINT('Ctrl Pts',(28.3054254819982,6.99176288834324,335.260527607764));
#16891=CARTESIAN_POINT('Ctrl Pts',(28.0271874477237,4.00272730963239,329.261463862102));
#16892=CARTESIAN_POINT('Ctrl Pts',(27.7489494134502,-2.6595520409677,328.528570029539));
#16893=CARTESIAN_POINT('Ctrl Pts',(27.5465709324433,-5.73019854909535,332.315077454903));
#16894=CARTESIAN_POINT('Ctrl Pts',(27.4369384628612,-5.92302912543987,334.636776519727));
#16895=CARTESIAN_POINT('Ctrl Pts',(27.4200520047038,-5.91977329940477,334.994921843694));
#16896=CARTESIAN_POINT('',(25.6700520047038,-5.90709767767298,334.999078370416));
#16897=CARTESIAN_POINT('Ctrl Pts',(27.4200520047038,-5.91977329940477,334.994921843694));
#16898=CARTESIAN_POINT('Ctrl Pts',(27.3441924514366,-5.90514705237084,336.603829053699));
#16899=CARTESIAN_POINT('Ctrl Pts',(27.1755868867448,-4.39436720596486,340.203961359681));
#16900=CARTESIAN_POINT('Ctrl Pts',(26.9142353106283,1.69899873852852,341.787195754337));
#16901=CARTESIAN_POINT('Ctrl Pts',(26.6359972763544,6.62692341423896,337.244216786105));
#16902=CARTESIAN_POINT('Ctrl Pts',(26.3577592420802,5.47341828593005,330.641753197846));
#16903=CARTESIAN_POINT('Ctrl Pts',(26.0795212078066,-0.70296201585298,328.038788372311));
#16904=CARTESIAN_POINT('Ctrl Pts',(25.8502854620142,-5.26009475152233,331.157382410602));
#16905=CARTESIAN_POINT('Ctrl Pts',(25.7137957276467,-5.90839173125013,334.066263377539));
#16906=CARTESIAN_POINT('Ctrl Pts',(25.6700520047038,-5.90709767767298,334.999078370416));
#16907=CARTESIAN_POINT('',(23.9200520047038,-5.91638134160122,335.005450646086));
#16908=CARTESIAN_POINT('Ctrl Pts',(25.6700520047038,-5.90709767767298,334.999078370416));
#16909=CARTESIAN_POINT('Ctrl Pts',(25.621049716222,-5.90564806199256,336.044029881305));
#16910=CARTESIAN_POINT('Ctrl Pts',(25.4793014163158,-5.1425470526809,339.068726244074));
#16911=CARTESIAN_POINT('Ctrl Pts',(25.2448071049846,-0.307755998838631,
341.989843286254));
#16912=CARTESIAN_POINT('Ctrl Pts',(24.9665690707106,5.71136391117128,339.041403864425));
#16913=CARTESIAN_POINT('Ctrl Pts',(24.6883310364366,6.48924945949215,332.384227767235));
#16914=CARTESIAN_POINT('Ctrl Pts',(24.4100930021627,1.31204655999919,328.127507239318));
#16915=CARTESIAN_POINT('Ctrl Pts',(24.1539999915853,-4.56131717805019,330.014406803911));
#16916=CARTESIAN_POINT('Ctrl Pts',(23.9906529924321,-5.9026043456772,333.505867600689));
#16917=CARTESIAN_POINT('Ctrl Pts',(23.9200520047038,-5.91638134160122,335.005450646086));
#16918=CARTESIAN_POINT('',(22.1700520047038,-5.92581566588214,334.998170041165));
#16919=CARTESIAN_POINT('Ctrl Pts',(23.9200520047038,-5.91638134160122,335.005450646086));
#16920=CARTESIAN_POINT('Ctrl Pts',(23.8979069810075,-5.92070269617454,335.475816616073));
#16921=CARTESIAN_POINT('Ctrl Pts',(23.7830159458868,-5.654242975896,337.911293734121));
#16922=CARTESIAN_POINT('Ctrl Pts',(23.5753788993408,-2.28893515882164,341.611610905065));
#16923=CARTESIAN_POINT('Ctrl Pts',(23.2971408650671,4.32117050908963,340.502736442224));
#16924=CARTESIAN_POINT('Ctrl Pts',(23.018902830793,6.96580178118044,334.344081966615));
#16925=CARTESIAN_POINT('Ctrl Pts',(22.7406647965191,3.21801957374706,328.787353788907));
#16926=CARTESIAN_POINT('Ctrl Pts',(22.4624267622454,-3.48289169861992,328.931879340613));
#16927=CARTESIAN_POINT('Ctrl Pts',(22.2722224983067,-5.8787228513342,332.837404167105));
#16928=CARTESIAN_POINT('Ctrl Pts',(22.1747642457929,-5.92621969426432,334.898494469636));
#16929=CARTESIAN_POINT('Ctrl Pts',(22.1700520047038,-5.92581566588214,334.998170041165));
#16930=CARTESIAN_POINT('',(20.4200532134703,-5.91336702896276,334.99550345961));
#16931=CARTESIAN_POINT('Ctrl Pts',(22.1700520047038,-5.92581566588214,334.998170041165));
#16932=CARTESIAN_POINT('Ctrl Pts',(22.0820182343683,-5.91826763488531,336.860302348495));
#16933=CARTESIAN_POINT('Ctrl Pts',(21.9012384526082,-3.96724156732265,340.697866670071));
#16934=CARTESIAN_POINT('Ctrl Pts',(21.6277126594233,2.57187304028365,341.506772778104));
#16935=CARTESIAN_POINT('Ctrl Pts',(21.3494746251494,6.86347212116061,336.358445200694));
#16936=CARTESIAN_POINT('Ctrl Pts',(21.0712365908757,4.85656414112844,329.963492513229));
#16937=CARTESIAN_POINT('Ctrl Pts',(20.7929985566017,-1.60714106844329,328.190468407641));
#16938=CARTESIAN_POINT('Ctrl Pts',(20.5759377291129,-5.49907885329114,331.682300406566));
#16939=CARTESIAN_POINT('Ctrl Pts',(20.4516229130488,-5.91556391747135,334.323369558575));
#16940=CARTESIAN_POINT('Ctrl Pts',(20.4200541084095,-5.91086361778023,334.995486298683));
#16941=CARTESIAN_POINT('',(18.6700508084278,-5.91273647904805,335.003866065122));
#16942=CARTESIAN_POINT('Ctrl Pts',(20.4200520047038,-5.91674830895615,334.995526638342));
#16943=CARTESIAN_POINT('Ctrl Pts',(20.4124049415101,-5.91687152346305,335.158497862473));
#16944=CARTESIAN_POINT('Ctrl Pts',(20.4047578783163,-5.91025650452325,335.321540234287));
#16945=CARTESIAN_POINT('Ctrl Pts',(20.3971108151226,-5.89691613023303,335.484056520974));
#16946=CARTESIAN_POINT('Ctrl Pts',(20.3897099568282,-5.88400526272547,335.641340432174));
#16947=CARTESIAN_POINT('Ctrl Pts',(20.3823090985338,-5.86479544317899,335.79813121691));
#16948=CARTESIAN_POINT('Ctrl Pts',(20.3749082402394,-5.83935123385778,335.953890837645));
#16949=CARTESIAN_POINT('Ctrl Pts',(20.3675067820282,-5.81390496201789,336.109663084323));
#16950=CARTESIAN_POINT('Ctrl Pts',(20.3601053238169,-5.78222335353899,336.264403633166));
#16951=CARTESIAN_POINT('Ctrl Pts',(20.3527038656057,-5.74442237470037,336.417583205156));
#16952=CARTESIAN_POINT('Ctrl Pts',(20.345300357778,-5.70661092799109,336.570805195729));
#16953=CARTESIAN_POINT('Ctrl Pts',(20.3378968499505,-5.66267682562992,336.722464987473));
#16954=CARTESIAN_POINT('Ctrl Pts',(20.3304933421228,-5.61278628424508,336.872047192218));
#16955=CARTESIAN_POINT('Ctrl Pts',(20.3230863340341,-5.56287215540371,337.021700117056));
#16956=CARTESIAN_POINT('Ctrl Pts',(20.3156793259455,-5.50699609746431,337.169273146422));
#16957=CARTESIAN_POINT('Ctrl Pts',(20.3082723178568,-5.44537289865636,337.314269767568));
#16958=CARTESIAN_POINT('Ctrl Pts',(20.3008563608104,-5.38367524827593,337.459441569922));
#16959=CARTESIAN_POINT('Ctrl Pts',(20.2934404037638,-5.3162167385794,337.602030406583));
#16960=CARTESIAN_POINT('Ctrl Pts',(20.2860244467174,-5.24325897864871,337.741562664854));
#16961=CARTESIAN_POINT('Ctrl Pts',(20.2786031501137,-5.1702486884591,337.881195387635));
#16962=CARTESIAN_POINT('Ctrl Pts',(20.27118185351,-5.09173144359106,338.017766825795));
#16963=CARTESIAN_POINT('Ctrl Pts',(20.2637605569062,-5.00801252846529,338.150831807195));
#16964=CARTESIAN_POINT('Ctrl Pts',(20.2563287610752,-4.92417517259198,338.284085041344));
#16965=CARTESIAN_POINT('Ctrl Pts',(20.2488969652442,-4.83512166474423,338.413821610219));
#16966=CARTESIAN_POINT('Ctrl Pts',(20.2414651694131,-4.74119832129923,338.53962837606));
#16967=CARTESIAN_POINT('Ctrl Pts',(20.23981760896,-4.72037638407118,338.567518573375));
#16968=CARTESIAN_POINT('Ctrl Pts',(20.2381700485069,-4.69931525608397,338.595215774627));
#16969=CARTESIAN_POINT('Ctrl Pts',(20.2365224880537,-4.67801895485086,338.622715724502));
#16970=CARTESIAN_POINT('Ctrl Pts',(20.2290985106158,-4.58205691620946,338.746631667637));
#16971=CARTESIAN_POINT('Ctrl Pts',(20.2216745331777,-4.48102310383591,338.866919006391));
#16972=CARTESIAN_POINT('Ctrl Pts',(20.2142505557397,-4.37522177053171,338.983135074431));
#16973=CARTESIAN_POINT('Ctrl Pts',(20.2068353397121,-4.26954529871933,339.099213990026));
#16974=CARTESIAN_POINT('Ctrl Pts',(20.1994201236846,-4.15911275420038,339.21123092547));
#16975=CARTESIAN_POINT('Ctrl Pts',(20.192004907657,-4.04427039495244,339.318773846245));
#16976=CARTESIAN_POINT('Ctrl Pts',(20.1845968265129,-3.92953853644458,339.426213289763));
#16977=CARTESIAN_POINT('Ctrl Pts',(20.1771887453688,-3.81040558102687,339.529187035419));
#16978=CARTESIAN_POINT('Ctrl Pts',(20.1697806642247,-3.68725653180423,339.627317779358));
#16979=CARTESIAN_POINT('Ctrl Pts',(20.1623780970507,-3.56419914466789,339.725375482793));
#16980=CARTESIAN_POINT('Ctrl Pts',(20.1549755298767,-3.43713190639008,339.818597130477));
#16981=CARTESIAN_POINT('Ctrl Pts',(20.1475729627027,-3.30647490142266,339.906643892597));
#16982=CARTESIAN_POINT('Ctrl Pts',(20.140174292948,-3.17588668679769,339.994644298482));
#16983=CARTESIAN_POINT('Ctrl Pts',(20.1327756231933,-3.04171277824053,340.077475036877));
#16984=CARTESIAN_POINT('Ctrl Pts',(20.1253769534385,-2.90440431301012,340.154839100211));
#16985=CARTESIAN_POINT('Ctrl Pts',(20.1179795042346,-2.76711849941242,340.232190400878));
#16986=CARTESIAN_POINT('Ctrl Pts',(20.1105820550306,-2.62669948026288,340.304076633305));
#16987=CARTESIAN_POINT('Ctrl Pts',(20.1031846058266,-2.4836253030275,340.370245424248));
#16988=CARTESIAN_POINT('Ctrl Pts',(20.0957874773632,-2.34055732923901,340.436411346228));
#16989=CARTESIAN_POINT('Ctrl Pts',(20.0883903488997,-2.19483476500656,340.496860162968));
#16990=CARTESIAN_POINT('Ctrl Pts',(20.0809932204363,-2.04695781771414,340.551386696583));
#16991=CARTESIAN_POINT('Ctrl Pts',(20.0735949529997,-1.89905810106313,340.605921625923));
#16992=CARTESIAN_POINT('Ctrl Pts',(20.066196685563,-1.74900369103808,340.654532327333));
#16993=CARTESIAN_POINT('Ctrl Pts',(20.0587984181264,-1.59731207189522,340.697062814072));
#16994=CARTESIAN_POINT('Ctrl Pts',(20.0513975516007,-1.44556716189089,340.739608242217));
#16995=CARTESIAN_POINT('Ctrl Pts',(20.0439966850749,-1.29218425673634,340.776069102143));
#16996=CARTESIAN_POINT('Ctrl Pts',(20.0365958185491,-1.13769305397936,340.806340075937));
#16997=CARTESIAN_POINT('Ctrl Pts',(20.0291868251643,-0.983032205112258,
340.836644290154));
#16998=CARTESIAN_POINT('Ctrl Pts',(20.0217778317796,-0.827260994660747,
340.860744972289));
#16999=CARTESIAN_POINT('Ctrl Pts',(20.0143688383948,-0.670917030464474,
340.878588342513));
#17000=CARTESIAN_POINT('Ctrl Pts',(20.0069552808146,-0.514476752992932,
340.896442704869));
#17001=CARTESIAN_POINT('Ctrl Pts',(19.9995417232344,-0.35746339003329,340.908032046865));
#17002=CARTESIAN_POINT('Ctrl Pts',(19.9921281656541,-0.200416108172359,
340.913354711675));
#17003=CARTESIAN_POINT('Ctrl Pts',(19.9847040535174,-0.0431452407550206,
340.918684954272));
#17004=CARTESIAN_POINT('Ctrl Pts',(19.9772799413807,0.114159269810065,340.917730703396));
#17005=CARTESIAN_POINT('Ctrl Pts',(19.969855829244,0.270960997063454,340.91054233557));
#17006=CARTESIAN_POINT('Ctrl Pts',(19.9659987040893,0.352425807314618,340.906807689076));
#17007=CARTESIAN_POINT('Ctrl Pts',(19.9621415789345,0.433755022734136,340.901391167795));
#17008=CARTESIAN_POINT('Ctrl Pts',(19.9582844537797,0.51487445884276,340.894305290204));
#17009=CARTESIAN_POINT('Ctrl Pts',(19.9508604763417,0.671008584465399,340.880666791776));
#17010=CARTESIAN_POINT('Ctrl Pts',(19.9434364989037,0.826835967036266,340.860799684575));
#17011=CARTESIAN_POINT('Ctrl Pts',(19.9360125214657,0.981819710343022,340.83472026912));
#17012=CARTESIAN_POINT('Ctrl Pts',(19.9285973054381,1.1366205495139,340.808671631299));
#17013=CARTESIAN_POINT('Ctrl Pts',(19.9211820894105,1.29057936676259,340.776425339938));
#17014=CARTESIAN_POINT('Ctrl Pts',(19.9137668733829,1.44316229341234,340.738049595235));
#17015=CARTESIAN_POINT('Ctrl Pts',(19.9063587922388,1.59559840553823,340.69971077548));
#17016=CARTESIAN_POINT('Ctrl Pts',(19.8989507110947,1.74666090313312,340.655254334086));
#17017=CARTESIAN_POINT('Ctrl Pts',(19.8915426299506,1.89582415606476,340.604799847611));
#17018=CARTESIAN_POINT('Ctrl Pts',(19.8841400627765,2.04487638406384,340.554382915332));
#17019=CARTESIAN_POINT('Ctrl Pts',(19.8767374956025,2.19203183014765,340.497976946422));
#17020=CARTESIAN_POINT('Ctrl Pts',(19.8693349284285,2.3367782332958,340.435751838605));
#17021=CARTESIAN_POINT('Ctrl Pts',(19.8619362586737,2.4814484280949,340.373559492035));
#17022=CARTESIAN_POINT('Ctrl Pts',(19.854537588919,2.62371176394598,340.305554255226));
#17023=CARTESIAN_POINT('Ctrl Pts',(19.8471389191642,2.76307434458884,340.231954771285));
#17024=CARTESIAN_POINT('Ctrl Pts',(19.8397414699602,2.90241393473314,340.158367428974));
#17025=CARTESIAN_POINT('Ctrl Pts',(19.8323440207563,3.03885338971015,340.07918784526));
#17026=CARTESIAN_POINT('Ctrl Pts',(19.8249465715523,3.17192178456038,339.994681446812));
#17027=CARTESIAN_POINT('Ctrl Pts',(19.8175494430888,3.30498440979718,339.910178712415));
#17028=CARTESIAN_POINT('Ctrl Pts',(19.8101523146254,3.43467595047803,339.820349822587));
#17029=CARTESIAN_POINT('Ctrl Pts',(19.8027551861619,3.56055317722488,339.725504378863));
#17030=CARTESIAN_POINT('Ctrl Pts',(19.7953569187253,3.68644978592178,339.630644331309));
#17031=CARTESIAN_POINT('Ctrl Pts',(19.7879586512887,3.8085306131858,339.530766416463));
#17032=CARTESIAN_POINT('Ctrl Pts',(19.7805603838521,3.92638444601334,339.4262213845));
#17033=CARTESIAN_POINT('Ctrl Pts',(19.7731595173264,4.04427968213241,339.321639624767));
#17034=CARTESIAN_POINT('Ctrl Pts',(19.7657586508006,4.15794468819,339.212387730971));
#17035=CARTESIAN_POINT('Ctrl Pts',(19.7583577842748,4.26700425037125,339.098854143515));
#17036=CARTESIAN_POINT('Ctrl Pts',(19.7509487908901,4.37618357037828,338.985195885326));
#17037=CARTESIAN_POINT('Ctrl Pts',(19.7435397975053,4.48074708827724,338.867246813225));
#17038=CARTESIAN_POINT('Ctrl Pts',(19.7361308041205,4.58035864901165,338.74542990976));
#17039=CARTESIAN_POINT('Ctrl Pts',(19.7287172465403,4.68003157390315,338.623537962881));
#17040=CARTESIAN_POINT('Ctrl Pts',(19.72130368896,4.77474623895761,338.497773734186));
#17041=CARTESIAN_POINT('Ctrl Pts',(19.7138901313798,4.86420947693562,338.368589723755));
#17042=CARTESIAN_POINT('Ctrl Pts',(19.7064660192431,4.95380008221146,338.239221796235));
#17043=CARTESIAN_POINT('Ctrl Pts',(19.6990419071064,5.03812412908979,338.106424677452));
#17044=CARTESIAN_POINT('Ctrl Pts',(19.6916177949697,5.11693368912605,337.970676721487));
#17045=CARTESIAN_POINT('Ctrl Pts',(19.6877606698151,5.15787842848923,337.900150193062));
#17046=CARTESIAN_POINT('Ctrl Pts',(19.6839035446605,5.1973354653187,337.82882753027));
#17047=CARTESIAN_POINT('Ctrl Pts',(19.6800464195059,5.23527518119148,337.75677789089));
#17048=CARTESIAN_POINT('Ctrl Pts',(19.6726224420679,5.30829941124691,337.618100799602));
#17049=CARTESIAN_POINT('Ctrl Pts',(19.6651984646299,5.37591987503774,337.476310997487));
#17050=CARTESIAN_POINT('Ctrl Pts',(19.6577744871919,5.43785973467028,337.331868793168));
#17051=CARTESIAN_POINT('Ctrl Pts',(19.6503592711643,5.4997264959491,337.187597052383));
#17052=CARTESIAN_POINT('Ctrl Pts',(19.6429440551367,5.55592585176677,337.040679479844));
#17053=CARTESIAN_POINT('Ctrl Pts',(19.6355288391091,5.60622624615212,336.891601924152));
#17054=CARTESIAN_POINT('Ctrl Pts',(19.628120757965,5.6564782417513,336.742667810133));
#17055=CARTESIAN_POINT('Ctrl Pts',(19.6207126768209,5.70084245715921,336.59157820178));
#17056=CARTESIAN_POINT('Ctrl Pts',(19.6133045956769,5.73913499823034,336.438839822422));
#17057=CARTESIAN_POINT('Ctrl Pts',(19.6059020285029,5.77739903746373,336.28621512903));
#17058=CARTESIAN_POINT('Ctrl Pts',(19.5984994613288,5.80960031049235,336.131944468644));
#17059=CARTESIAN_POINT('Ctrl Pts',(19.5910968941548,5.83560447410472,335.976550553893));
#17060=CARTESIAN_POINT('Ctrl Pts',(19.5836982244,5.86159494663883,335.821238453358));
#17061=CARTESIAN_POINT('Ctrl Pts',(19.5762995546453,5.88139474627604,335.664804643408));
#17062=CARTESIAN_POINT('Ctrl Pts',(19.5689008848905,5.89492045906299,335.507782772276));
#17063=CARTESIAN_POINT('Ctrl Pts',(19.5615034356866,5.90844394052725,335.350786804879));
#17064=CARTESIAN_POINT('Ctrl Pts',(19.5541059864825,5.91569535734219,335.193203340309));
#17065=CARTESIAN_POINT('Ctrl Pts',(19.5467085372786,5.9166430679393,335.035572027014));
#17066=CARTESIAN_POINT('Ctrl Pts',(19.5393114088151,5.91759073744532,334.877947548338));
#17067=CARTESIAN_POINT('Ctrl Pts',(19.5319142803517,5.9122352419354,334.720275598266));
#17068=CARTESIAN_POINT('Ctrl Pts',(19.5245171518882,5.90059707509556,334.563096440992));
#17069=CARTESIAN_POINT('Ctrl Pts',(19.5171188844516,5.88895711626851,334.405893082052));
#17070=CARTESIAN_POINT('Ctrl Pts',(19.5097206170149,5.87103258750171,334.249183039208));
#17071=CARTESIAN_POINT('Ctrl Pts',(19.5023223495783,5.84689591114812,334.093501921293));
#17072=CARTESIAN_POINT('Ctrl Pts',(19.4949214830525,5.82275075532633,333.937766110965));
#17073=CARTESIAN_POINT('Ctrl Pts',(19.4875206165268,5.79238916392071,333.783060313829));
#17074=CARTESIAN_POINT('Ctrl Pts',(19.480119750001,5.75593473502909,333.629910262579));
#17075=CARTESIAN_POINT('Ctrl Pts',(19.4727107566163,5.71944027568943,333.476592037932));
#17076=CARTESIAN_POINT('Ctrl Pts',(19.4653017632315,5.6768397040147,333.324833334135));
#17077=CARTESIAN_POINT('Ctrl Pts',(19.4578927698468,5.62830680226529,333.175145731278));
#17078=CARTESIAN_POINT('Ctrl Pts',(19.4504792122666,5.57974400257445,333.025365915694));
#17079=CARTESIAN_POINT('Ctrl Pts',(19.4430656546863,5.52524171959014,332.877660092704));
#17080=CARTESIAN_POINT('Ctrl Pts',(19.4356520971061,5.4650218206688,332.732519666653));
#17081=CARTESIAN_POINT('Ctrl Pts',(19.4282279849694,5.40471618769645,332.587172606634));
#17082=CARTESIAN_POINT('Ctrl Pts',(19.4208038728328,5.33867683768847,332.444398575769));
#17083=CARTESIAN_POINT('Ctrl Pts',(19.4133797606961,5.26717186048937,332.304664927218));
#17084=CARTESIAN_POINT('Ctrl Pts',(19.4095226355414,5.2300221459965,332.232067671026));
#17085=CARTESIAN_POINT('Ctrl Pts',(19.4056655103867,5.19139786392455,332.160290621645));
#17086=CARTESIAN_POINT('Ctrl Pts',(19.401808385232,5.15134114229636,332.089396111082));
#17087=CARTESIAN_POINT('Ctrl Pts',(19.394384407794,5.07424221869873,331.952942346739));
#17088=CARTESIAN_POINT('Ctrl Pts',(19.3869604303559,4.99160146216521,331.819348258295));
#17089=CARTESIAN_POINT('Ctrl Pts',(19.3795364529179,4.90365614316965,331.689095744052));
#17090=CARTESIAN_POINT('Ctrl Pts',(19.3721212368903,4.8158146128826,331.558996947373));
#17091=CARTESIAN_POINT('Ctrl Pts',(19.3647060208627,4.72268118793632,331.432232181476));
#17092=CARTESIAN_POINT('Ctrl Pts',(19.357290804835,4.62453912056222,331.309259087271));
#17093=CARTESIAN_POINT('Ctrl Pts',(19.3498827236909,4.52649148499099,331.186404317159));
#17094=CARTESIAN_POINT('Ctrl Pts',(19.3424746425467,4.4234450325462,331.067334245353));
#17095=CARTESIAN_POINT('Ctrl Pts',(19.3350665614026,4.31572636201215,330.952477729433));
#17096=CARTESIAN_POINT('Ctrl Pts',(19.3276639942286,4.20808786845238,330.837706703317));
#17097=CARTESIAN_POINT('Ctrl Pts',(19.3202614270546,4.0957843354581,330.727143259459));
#17098=CARTESIAN_POINT('Ctrl Pts',(19.3128588598806,3.97918262240907,330.62118323973));
#17099=CARTESIAN_POINT('Ctrl Pts',(19.3054601901259,3.86264229965235,330.515279007489));
#17100=CARTESIAN_POINT('Ctrl Pts',(19.2980615203711,3.74180857919321,330.41397362283));
#17101=CARTESIAN_POINT('Ctrl Pts',(19.2906628506164,3.61708507713897,330.317626018008));
#17102=CARTESIAN_POINT('Ctrl Pts',(19.2832654014124,3.49238215058916,330.221294307548));
#17103=CARTESIAN_POINT('Ctrl Pts',(19.2758679522084,3.36379101106114,330.12991898163));
#17104=CARTESIAN_POINT('Ctrl Pts',(19.2684705030044,3.23174833737776,330.043818683063));
#17105=CARTESIAN_POINT('Ctrl Pts',(19.261073374541,3.09971138883507,329.957722117655));
#17106=CARTESIAN_POINT('Ctrl Pts',(19.2536762460775,2.96422351631697,329.876900328686));
#17107=CARTESIAN_POINT('Ctrl Pts',(19.246279117614,2.82575012982042,329.801628450532));
#17108=CARTESIAN_POINT('Ctrl Pts',(19.2388808501774,2.68725542187853,329.726344982388));
#17109=CARTESIAN_POINT('Ctrl Pts',(19.2314825827407,2.54577461256367,329.656613304827));
#17110=CARTESIAN_POINT('Ctrl Pts',(19.2240843153041,2.40179729866099,329.592662365022));
#17111=CARTESIAN_POINT('Ctrl Pts',(19.2166834487783,2.25776940401343,329.52868895858));
#17112=CARTESIAN_POINT('Ctrl Pts',(19.2092825822525,2.11124359944051,329.470500484682));
#17113=CARTESIAN_POINT('Ctrl Pts',(19.2018817157267,1.96272887080264,329.418277511178));
#17114=CARTESIAN_POINT('Ctrl Pts',(19.194472722342,1.8140510587948,329.365997191858));
#17115=CARTESIAN_POINT('Ctrl Pts',(19.1870637289571,1.66338031338868,329.319695578886));
#17116=CARTESIAN_POINT('Ctrl Pts',(19.1796547355724,1.5112408767462,329.279503380392));
#17117=CARTESIAN_POINT('Ctrl Pts',(19.1722411779921,1.35900771696247,329.239286422117));
#17118=CARTESIAN_POINT('Ctrl Pts',(19.1648276204119,1.20530442658057,329.205186458456));
#17119=CARTESIAN_POINT('Ctrl Pts',(19.1574140628316,1.05066430315455,329.177282843502));
#17120=CARTESIAN_POINT('Ctrl Pts',(19.1499899506949,0.895804021202609,329.149339502644));
#17121=CARTESIAN_POINT('Ctrl Pts',(19.1425658385582,0.740004611070968,329.127610180481));
#17122=CARTESIAN_POINT('Ctrl Pts',(19.1351417264215,0.583804158799896,329.112122346153));
#17123=CARTESIAN_POINT('Ctrl Pts',(19.1312846012669,0.502651735115012,329.10407579267));
#17124=CARTESIAN_POINT('Ctrl Pts',(19.1274274761125,0.421391067708476,329.097713095492));
#17125=CARTESIAN_POINT('Ctrl Pts',(19.1235703509579,0.340097370784199,329.09303255969));
#17126=CARTESIAN_POINT('Ctrl Pts',(19.1161463735199,0.183627837740699,329.084023727775));
#17127=CARTESIAN_POINT('Ctrl Pts',(19.1087223960819,0.026564063377994,329.081222676123));
#17128=CARTESIAN_POINT('Ctrl Pts',(19.1012984186439,-0.130560313074239,
329.084690661753));
#17129=CARTESIAN_POINT('Ctrl Pts',(19.0938832026163,-0.287499259121399,
329.088154554638));
#17130=CARTESIAN_POINT('Ctrl Pts',(19.0864679865887,-0.444498295405287,
329.097872750002));
#17131=CARTESIAN_POINT('Ctrl Pts',(19.079052770561,-0.601019297883888,329.113854710758));
#17132=CARTESIAN_POINT('Ctrl Pts',(19.0716446894169,-0.757389696642328,
329.129821293751));
#17133=CARTESIAN_POINT('Ctrl Pts',(19.0642366082728,-0.913282608494122,
329.152039605918));
#17134=CARTESIAN_POINT('Ctrl Pts',(19.0568285271287,-1.0681606566089,329.180467082817));
#17135=CARTESIAN_POINT('Ctrl Pts',(19.0494259599547,-1.22292342616362,329.208873400626));
#17136=CARTESIAN_POINT('Ctrl Pts',(19.0420233927807,-1.37667247054935,329.243479613812));
#17137=CARTESIAN_POINT('Ctrl Pts',(19.0346208256067,-1.52887638923313,329.284191435243));
#17138=CARTESIAN_POINT('Ctrl Pts',(19.0272221558519,-1.68100017321957,329.324881822079));
#17139=CARTESIAN_POINT('Ctrl Pts',(19.0198234860972,-1.83158009201295,329.371671318947));
#17140=CARTESIAN_POINT('Ctrl Pts',(19.0124248163424,-1.9800958919896,329.42441475529));
#17141=CARTESIAN_POINT('Ctrl Pts',(19.0050273671384,-2.12858719147049,329.477149490604));
#17142=CARTESIAN_POINT('Ctrl Pts',(18.9976299179345,-2.2750146965983,329.535836091235));
#17143=CARTESIAN_POINT('Ctrl Pts',(18.9902324687305,-2.41887414186912,329.600279780554));
#17144=CARTESIAN_POINT('Ctrl Pts',(18.982835340267,-2.5627273496452,329.664720675706));
#17145=CARTESIAN_POINT('Ctrl Pts',(18.9754382118034,-2.70401237835945,329.734918010649));
#17146=CARTESIAN_POINT('Ctrl Pts',(18.96804108334,-2.84224600158876,329.810629303186));
#17147=CARTESIAN_POINT('Ctrl Pts',(18.9606428159034,-2.98050090934507,329.886352253372));
#17148=CARTESIAN_POINT('Ctrl Pts',(18.9532445484668,-3.11570314875237,329.967590672354));
#17149=CARTESIAN_POINT('Ctrl Pts',(18.9458462810302,-3.24739524433666,330.054056744203));
#17150=CARTESIAN_POINT('Ctrl Pts',(18.9384454145044,-3.37913360473959,330.140553192493));
#17151=CARTESIAN_POINT('Ctrl Pts',(18.9310445479786,-3.50735905433997,330.232280745469));
#17152=CARTESIAN_POINT('Ctrl Pts',(18.9236436814528,-3.63164430832625,330.328909101687));
#17153=CARTESIAN_POINT('Ctrl Pts',(18.9162346880681,-3.75606603940354,330.425643565078));
#17154=CARTESIAN_POINT('Ctrl Pts',(18.9088256946833,-3.87653863937833,330.527289349745));
#17155=CARTESIAN_POINT('Ctrl Pts',(18.9014167012985,-3.99266849548134,330.633476342937));
#17156=CARTESIAN_POINT('Ctrl Pts',(18.8940031437182,-4.1088698915813,330.73972875098));
#17157=CARTESIAN_POINT('Ctrl Pts',(18.886589586138,-4.22072294843319,330.850527679985));
#17158=CARTESIAN_POINT('Ctrl Pts',(18.8791760285577,-4.32787233757927,330.965467611716));
#17159=CARTESIAN_POINT('Ctrl Pts',(18.871751916421,-4.43517427349696,331.080571181481));
#17160=CARTESIAN_POINT('Ctrl Pts',(18.8643278042844,-4.5377589246694,331.199827246245));
#17161=CARTESIAN_POINT('Ctrl Pts',(18.8569036921477,-4.63531200247758,331.322798183103));
#17162=CARTESIAN_POINT('Ctrl Pts',(18.8530465669932,-4.68599475394827,331.38668653569));
#17163=CARTESIAN_POINT('Ctrl Pts',(18.8491894418386,-4.73532009161764,331.451577143998));
#17164=CARTESIAN_POINT('Ctrl Pts',(18.8453323166841,-4.78324873806546,331.517405841575));
#17165=CARTESIAN_POINT('Ctrl Pts',(18.8378562134419,-4.87614681493517,331.644998833679));
#17166=CARTESIAN_POINT('Ctrl Pts',(18.8303801101998,-4.96407508132413,331.776502304084));
#17167=CARTESIAN_POINT('Ctrl Pts',(18.8229040069576,-5.04668908599542,331.911495534762));
#17168=CARTESIAN_POINT('Ctrl Pts',(18.8154369210783,-5.12920344511252,332.046325942256));
#17169=CARTESIAN_POINT('Ctrl Pts',(18.8079698351989,-5.20641611232975,332.184637422512));
#17170=CARTESIAN_POINT('Ctrl Pts',(18.8005027493195,-5.27802363396329,332.325977359515));
#17171=CARTESIAN_POINT('Ctrl Pts',(18.7930432660791,-5.34955824815441,332.46717339078));
#17172=CARTESIAN_POINT('Ctrl Pts',(18.7855837828386,-5.4154989140809,332.611391415902));
#17173=CARTESIAN_POINT('Ctrl Pts',(18.7781242995982,-5.47558619588623,332.758151125985));
#17174=CARTESIAN_POINT('Ctrl Pts',(18.7706710092691,-5.53562359284104,332.904788995207));
#17175=CARTESIAN_POINT('Ctrl Pts',(18.76321771894,-5.58981714403671,333.053964010386));
#17176=CARTESIAN_POINT('Ctrl Pts',(18.7557644286108,-5.6379540075695,333.205172662613));
#17177=CARTESIAN_POINT('Ctrl Pts',(18.7483162710588,-5.68605772120779,333.356277183609));
#17178=CARTESIAN_POINT('Ctrl Pts',(18.7408681135067,-5.72811294622758,333.50941220359));
#17179=CARTESIAN_POINT('Ctrl Pts',(18.7334199559546,-5.76395556104348,333.664055819723));
#17180=CARTESIAN_POINT('Ctrl Pts',(18.7259748909015,-5.79978329389037,333.818635227329));
#17181=CARTESIAN_POINT('Ctrl Pts',(18.7185298258484,-5.82940347153863,333.974721627405));
#17182=CARTESIAN_POINT('Ctrl Pts',(18.7110847607953,-5.85270226027492,334.131779512409));
#17183=CARTESIAN_POINT('Ctrl Pts',(18.7036403547161,-5.87599898680061,334.288823495985));
#17184=CARTESIAN_POINT('Ctrl Pts',(18.6961959486368,-5.89297537834226,334.446838432158));
#17185=CARTESIAN_POINT('Ctrl Pts',(18.6887515425575,-5.9035689811631,334.605280039586));
#17186=CARTESIAN_POINT('Ctrl Pts',(18.6825183632729,-5.91243897360421,334.737942730836));
#17187=CARTESIAN_POINT('Ctrl Pts',(18.6762851839884,-5.91683510150182,334.870904283113));
#17188=CARTESIAN_POINT('Ctrl Pts',(18.6700520047038,-5.91674875184026,335.003843188353));
#17189=CARTESIAN_POINT('',(16.9200520047038,-5.92487683695815,335.002801334899));
#17190=CARTESIAN_POINT('Ctrl Pts',(18.6700498739345,-5.9096022173903,335.003883935737));
#17191=CARTESIAN_POINT('Ctrl Pts',(18.6357313434263,-5.91393132263513,335.734935624386));
#17192=CARTESIAN_POINT('Ctrl Pts',(18.5086668014939,-5.4490096090293,338.436336667853));
#17193=CARTESIAN_POINT('Ctrl Pts',(18.288856248136,-1.40478184172838,341.854138231637));
#17194=CARTESIAN_POINT('Ctrl Pts',(18.0106182138624,5.00358300468427,339.890478507921));
#17195=CARTESIAN_POINT('Ctrl Pts',(17.7323801795881,6.82023358046314,333.438898840832));
#17196=CARTESIAN_POINT('Ctrl Pts',(17.4541421453145,2.37805646593319,328.419918665697));
#17197=CARTESIAN_POINT('Ctrl Pts',(17.1833660870195,-4.06876805880988,329.412041351052));
#17198=CARTESIAN_POINT('Ctrl Pts',(17.0053360401494,-5.91432262045667,333.198073718685));
#17199=CARTESIAN_POINT('Ctrl Pts',(16.9200520047038,-5.92487683695815,335.002801334899));
#17200=CARTESIAN_POINT('',(15.1700520047038,-5.91816246639694,334.994658507115));
#17201=CARTESIAN_POINT('Ctrl Pts',(16.9200520047038,-5.92487683695815,335.002801334899));
#17202=CARTESIAN_POINT('Ctrl Pts',(16.9125900287247,-5.92580028423173,335.160707020889));
#17203=CARTESIAN_POINT('Ctrl Pts',(16.9051280527456,-5.92003632359302,335.318544233041));
#17204=CARTESIAN_POINT('Ctrl Pts',(16.8049200653418,-5.74990729362354,337.430694969049));
#17205=CARTESIAN_POINT('Ctrl Pts',(16.6194280424926,-3.30166561657978,341.168600090581));
#17206=CARTESIAN_POINT('Ctrl Pts',(16.3411900082185,3.40058670281529,341.114624518141));
#17207=CARTESIAN_POINT('Ctrl Pts',(16.0629519739446,6.98217079761695,335.449348277112));
#17208=CARTESIAN_POINT('Ctrl Pts',(15.7847139396707,4.15631980811429,329.371711754549));
#17209=CARTESIAN_POINT('Ctrl Pts',(15.5064759053968,-2.48372452211122,328.459072281435));
#17210=CARTESIAN_POINT('Ctrl Pts',(15.3015885937412,-5.69488085772441,332.207123730002));
#17211=CARTESIAN_POINT('Ctrl Pts',(15.1894472935101,-5.92197975965578,334.583014993244));
#17212=CARTESIAN_POINT('Ctrl Pts',(15.1700520047038,-5.91816246639694,334.994658507115));
#17213=CARTESIAN_POINT('',(13.4200520047038,-5.90696799723574,334.999957581698));
#17214=CARTESIAN_POINT('Ctrl Pts',(15.1700520047038,-5.91816246639694,334.994658507115));
#17215=CARTESIAN_POINT('Ctrl Pts',(15.0967012820855,-5.90372590802558,336.551446318067));
#17216=CARTESIAN_POINT('Ctrl Pts',(14.9306045480426,-4.47531169421653,340.100099714576));
#17217=CARTESIAN_POINT('Ctrl Pts',(14.671761802575,1.51499000097043,341.830624291977));
#17218=CARTESIAN_POINT('Ctrl Pts',(14.3935237683009,6.56386571174399,337.422455332818));
#17219=CARTESIAN_POINT('Ctrl Pts',(14.115285734027,5.5891787413283,330.791234870104));
#17220=CARTESIAN_POINT('Ctrl Pts',(13.8370476997532,-0.5146150638219,328.022336045841));
#17221=CARTESIAN_POINT('Ctrl Pts',(13.6053031233121,-5.20512640970425,331.049429673258));
#17222=CARTESIAN_POINT('Ctrl Pts',(13.4663045582956,-5.90703089584316,334.013588927452));
#17223=CARTESIAN_POINT('Ctrl Pts',(13.4200520047038,-5.90696799723574,334.999957581698));
#17224=CARTESIAN_POINT('',(11.6700520047038,-5.91800630270739,335.005358570736));
#17225=CARTESIAN_POINT('Ctrl Pts',(13.4200520047038,-5.90696799723574,334.999957581698));
#17226=CARTESIAN_POINT('Ctrl Pts',(13.373558546871,-5.90690477102391,335.991463690498));
#17227=CARTESIAN_POINT('Ctrl Pts',(13.2343190776133,-5.19974192404982,338.960929310428));
#17228=CARTESIAN_POINT('Ctrl Pts',(13.0023335969315,-0.496507558018799,
341.978975796318));
#17229=CARTESIAN_POINT('Ctrl Pts',(12.7240955626572,5.60008090817167,339.194248054982));
#17230=CARTESIAN_POINT('Ctrl Pts',(12.4458575283836,6.55755778108378,332.560520780316));
#17231=CARTESIAN_POINT('Ctrl Pts',(12.1676194941094,1.49726066940123,328.165467579416));
#17232=CARTESIAN_POINT('Ctrl Pts',(11.909017652883,-4.48295950437942,329.909905021892));
#17233=CARTESIAN_POINT('Ctrl Pts',(11.7431618230811,-5.90360988232098,333.453578574384));
#17234=CARTESIAN_POINT('Ctrl Pts',(11.6700520047038,-5.91800630270739,335.005358570736));
#17235=CARTESIAN_POINT('',(9.92005200470384,-5.92497233409181,334.997279528669));
#17236=CARTESIAN_POINT('Ctrl Pts',(11.6700520047038,-5.91800630270739,335.005358570736));
#17237=CARTESIAN_POINT('Ctrl Pts',(11.6504158116564,-5.92187296379579,335.422143241411));
#17238=CARTESIAN_POINT('Ctrl Pts',(11.5380336071844,-5.69140174168275,337.803246946089));
#17239=CARTESIAN_POINT('Ctrl Pts',(11.3329053912876,-2.46674364463169,341.54735051138));
#17240=CARTESIAN_POINT('Ctrl Pts',(11.0546673570137,4.17091021541455,340.617484404395));
#17241=CARTESIAN_POINT('Ctrl Pts',(10.77642932274,6.98098129236843,334.532535761013));
#17242=CARTESIAN_POINT('Ctrl Pts',(10.4981912884658,3.38470895373127,328.876572173443));
#17243=CARTESIAN_POINT('Ctrl Pts',(10.219953254192,-3.31766097947469,328.839987876369));
#17244=CARTESIAN_POINT('Ctrl Pts',(10.0272401596045,-5.85112546410686,332.729993995301));
#17245=CARTESIAN_POINT('Ctrl Pts',(9.92727307644188,-5.92584438465563,334.844478228084));
#17246=CARTESIAN_POINT('Ctrl Pts',(9.92005200470384,-5.92497233409181,334.997279528669));
#17247=CARTESIAN_POINT('',(8.17005320238592,-5.91279716752603,334.996073171796));
#17248=CARTESIAN_POINT('Ctrl Pts',(9.92005200470384,-5.92497233409181,334.997279528669));
#17249=CARTESIAN_POINT('Ctrl Pts',(9.83452706501725,-5.9146439403879,336.807027789136));
#17250=CARTESIAN_POINT('Ctrl Pts',(9.6562561139059,-4.05999276733219,340.597629687215));
#17251=CARTESIAN_POINT('Ctrl Pts',(9.38523915137018,2.39512310876783,341.573888717416));
#17252=CARTESIAN_POINT('Ctrl Pts',(9.10700111709619,6.8242603936016,336.543398329723));
#17253=CARTESIAN_POINT('Ctrl Pts',(8.82876308282223,4.99087814415887,330.096555138453));
#17254=CARTESIAN_POINT('Ctrl Pts',(8.55052504854831,-1.42256592733979,328.149528914564));
#17255=CARTESIAN_POINT('Ctrl Pts',(8.3309554007549,-5.45348075719915,331.574058185186));
#17256=CARTESIAN_POINT('Ctrl Pts',(8.20413176438612,-5.91407537989431,334.270167138421));
#17257=CARTESIAN_POINT('Ctrl Pts',(8.17005413944201,-5.90970551307915,334.996055251526));
#17258=CARTESIAN_POINT('',(6.4200506595843,-5.91295548729207,335.00439982517));
#17259=CARTESIAN_POINT('Ctrl Pts',(8.1700520047039,-5.91674871207825,334.996096076278));
#17260=CARTESIAN_POINT('Ctrl Pts',(8.16261128968737,-5.91685341255526,335.154779097913));
#17261=CARTESIAN_POINT('Ctrl Pts',(8.15517057467084,-5.91057013696326,335.313497435384));
#17262=CARTESIAN_POINT('Ctrl Pts',(8.14772985965431,-5.89791707973895,335.471704020572));
#17263=CARTESIAN_POINT('Ctrl Pts',(8.14028890613604,-5.88526361693856,335.629915676851));
#17264=CARTESIAN_POINT('Ctrl Pts',(8.13284795261774,-5.86623999404314,335.787615182283));
#17265=CARTESIAN_POINT('Ctrl Pts',(8.12540699909948,-5.84091638686498,335.944259669875));
#17266=CARTESIAN_POINT('Ctrl Pts',(8.11796440350357,-5.81558719124586,336.100938725942));
#17267=CARTESIAN_POINT('Ctrl Pts',(8.11052180790766,-5.78395530032008,336.256561938121));
#17268=CARTESIAN_POINT('Ctrl Pts',(8.10307921231174,-5.74614219166644,336.410595787478));
#17269=CARTESIAN_POINT('Ctrl Pts',(8.09563357036449,-5.70831360561479,336.564692684897));
#17270=CARTESIAN_POINT('Ctrl Pts',(8.08818792841724,-5.66429884968457,336.717198567574));
#17271=CARTESIAN_POINT('Ctrl Pts',(8.08074228646998,-5.61426950163742,336.867594315017));
#17272=CARTESIAN_POINT('Ctrl Pts',(8.0732873930601,-5.56417799042865,337.018176934277));
#17273=CARTESIAN_POINT('Ctrl Pts',(8.06583249965017,-5.50805707313053,337.166643831786));
#17274=CARTESIAN_POINT('Ctrl Pts',(8.05837760624027,-5.44612715732812,337.312494226742));
#17275=CARTESIAN_POINT('Ctrl Pts',(8.05091788039282,-5.38415709709514,337.458439165359));
#17276=CARTESIAN_POINT('Ctrl Pts',(8.04345815454545,-5.31637068928892,337.60176388955));
#17277=CARTESIAN_POINT('Ctrl Pts',(8.03599842869801,-5.24303453243653,337.741991877117));
#17278=CARTESIAN_POINT('Ctrl Pts',(8.02852639187366,-5.16957734704341,337.882451286529));
#17279=CARTESIAN_POINT('Ctrl Pts',(8.02105435504934,-5.09055229266335,338.019803428556));
#17280=CARTESIAN_POINT('Ctrl Pts',(8.01358231822499,-5.00627021212153,338.15359939208));
#17281=CARTESIAN_POINT('Ctrl Pts',(8.00707120548348,-4.9328270343914,338.270188833934));
#17282=CARTESIAN_POINT('Ctrl Pts',(8.00056009274194,-4.85539278182729,338.384078304153));
#17283=CARTESIAN_POINT('Ctrl Pts',(7.99404898000043,-4.77419758737321,338.49499183965));
#17284=CARTESIAN_POINT('Ctrl Pts',(7.98662520049577,-4.68162121150709,338.621452195092));
#17285=CARTESIAN_POINT('Ctrl Pts',(7.97920142099114,-4.58387709032002,338.744422551539));
#17286=CARTESIAN_POINT('Ctrl Pts',(7.97177764148648,-4.48125737924786,338.86345219505));
#17287=CARTESIAN_POINT('Ctrl Pts',(7.96436262351687,-4.37875877982704,338.982341359928));
#17288=CARTESIAN_POINT('Ctrl Pts',(7.95694760554722,-4.27139628560484,339.09729878947));
#17289=CARTESIAN_POINT('Ctrl Pts',(7.94953258757761,-4.15950487043829,339.207903254033));
#17290=CARTESIAN_POINT('Ctrl Pts',(7.94212470443006,-4.04772111857621,339.318401293611));
#17291=CARTESIAN_POINT('Ctrl Pts',(7.93471682128259,-3.93141738495927,339.424554446049));
#17292=CARTESIAN_POINT('Ctrl Pts',(7.92730893813504,-3.81096831371177,339.525975151764));
#17293=CARTESIAN_POINT('Ctrl Pts',(7.91990656871137,-3.69060889330077,339.627320369549));
#17294=CARTESIAN_POINT('Ctrl Pts',(7.91250419928765,-3.56611056300302,339.723939914813));
#17295=CARTESIAN_POINT('Ctrl Pts',(7.90510182986398,-3.43788407581089,339.815483739334));
#17296=CARTESIAN_POINT('Ctrl Pts',(7.89770335742933,-3.30972509365438,339.906979370464));
#17297=CARTESIAN_POINT('Ctrl Pts',(7.89030488499471,-3.17784216642058,339.993404386215));
#17298=CARTESIAN_POINT('Ctrl Pts',(7.88290641256006,-3.04267821921571,340.074449705812));
#17299=CARTESIAN_POINT('Ctrl Pts',(7.87550915941151,-2.90753654735533,340.155481668944));
#17300=CARTESIAN_POINT('Ctrl Pts',(7.86811190626295,-2.76911524845875,340.231135503748));
#17301=CARTESIAN_POINT('Ctrl Pts',(7.8607146531144,-2.62788535456432,340.301146020038));
#17302=CARTESIAN_POINT('Ctrl Pts',(7.85331771990311,-2.48666156897862,340.371153508316));
#17303=CARTESIAN_POINT('Ctrl Pts',(7.84592078669181,-2.34262976432439,340.435517997615));
#17304=CARTESIAN_POINT('Ctrl Pts',(7.83852385348052,-2.19628439986807,340.494020877044));
#17305=CARTESIAN_POINT('Ctrl Pts',(7.83112578032705,-2.04991648211161,340.552532772358));
#17306=CARTESIAN_POINT('Ctrl Pts',(7.82372770717357,-1.90123464121756,340.605181120595));
#17307=CARTESIAN_POINT('Ctrl Pts',(7.81632963402009,-1.75075193607407,340.65179601727));
#17308=CARTESIAN_POINT('Ctrl Pts',(7.80892896064176,-1.60021634028417,340.698427297835));
#17309=CARTESIAN_POINT('Ctrl Pts',(7.80152828726342,-1.44787897632691,340.739020794368));
#17310=CARTESIAN_POINT('Ctrl Pts',(7.79412761388508,-1.29426648061765,340.773456922819));
#17311=CARTESIAN_POINT('Ctrl Pts',(7.78671881095491,-1.14048524340577,340.807930878948));
#17312=CARTESIAN_POINT('Ctrl Pts',(7.77931000802474,-0.985426441546715,
340.836233877646));
#17313=CARTESIAN_POINT('Ctrl Pts',(7.77190120509457,-0.829626011028604,
340.858297640469));
#17314=CARTESIAN_POINT('Ctrl Pts',(7.76448783672733,-0.673729573494713,
340.880374999378));
#17315=CARTESIAN_POINT('Ctrl Pts',(7.7570744683601,-0.517090967133179,340.896205423853));
#17316=CARTESIAN_POINT('Ctrl Pts',(7.74966109999286,-0.360249093448792,
340.905772697384));
#17317=CARTESIAN_POINT('Ctrl Pts',(7.74223717350793,-0.203183845600268,
340.915353596625));
#17318=CARTESIAN_POINT('Ctrl Pts',(7.734813247023,-0.0459151243963421,340.918653522137));
#17319=CARTESIAN_POINT('Ctrl Pts',(7.72738932053807,0.111019502717101,340.915708345796));
#17320=CARTESIAN_POINT('Ctrl Pts',(7.72352986226756,0.192604718541949,340.914177244267));
#17321=CARTESIAN_POINT('Ctrl Pts',(7.71967040399709,0.274099735862142,340.910959182106));
#17322=CARTESIAN_POINT('Ctrl Pts',(7.71581094572659,0.355429922037766,340.906064690894));
#17323=CARTESIAN_POINT('Ctrl Pts',(7.70838684006637,0.511877758291882,340.896649581992));
#17324=CARTESIAN_POINT('Ctrl Pts',(7.70096273440614,0.668187230436248,340.880999674986));
#17325=CARTESIAN_POINT('Ctrl Pts',(7.69353862874593,0.823821184575319,340.859116760941));
#17326=CARTESIAN_POINT('Ctrl Pts',(7.68612328556047,0.979271448091348,340.837259674719));
#17327=CARTESIAN_POINT('Ctrl Pts',(7.67870794237503,1.13404741466381,340.809184276456));
#17328=CARTESIAN_POINT('Ctrl Pts',(7.67129259918957,1.28761355480564,340.77494431973));
#17329=CARTESIAN_POINT('Ctrl Pts',(7.66388439205692,1.44103191269953,340.740737313351));
#17330=CARTESIAN_POINT('Ctrl Pts',(7.65647618492427,1.59324240016855,340.700377639446));
#17331=CARTESIAN_POINT('Ctrl Pts',(7.64906797779162,1.74371633521224,340.653970631761));
#17332=CARTESIAN_POINT('Ctrl Pts',(7.64166528590329,1.89407824578052,340.607598173054));
#17333=CARTESIAN_POINT('Ctrl Pts',(7.63426259401497,2.04270582303051,340.555187454431));
#17334=CARTESIAN_POINT('Ctrl Pts',(7.62685990212665,2.18908238948749,340.496894473658));
#17335=CARTESIAN_POINT('Ctrl Pts',(7.61946110903723,2.33538186334032,340.438632194232));
#17336=CARTESIAN_POINT('Ctrl Pts',(7.61206231594777,2.47943234164554,340.374493960295));
#17337=CARTESIAN_POINT('Ctrl Pts',(7.60466352285835,2.62073418769751,340.304684993469));
#17338=CARTESIAN_POINT('Ctrl Pts',(7.59726595275613,2.76201267719003,340.234887565751));
#17339=CARTESIAN_POINT('Ctrl Pts',(7.58986838265393,2.90054310188425,340.159421430637));
#17340=CARTESIAN_POINT('Ctrl Pts',(7.58247081255172,3.03584752374562,340.078539196961));
#17341=CARTESIAN_POINT('Ctrl Pts',(7.57507356471138,3.1711460513126,339.997660486775));
#17342=CARTESIAN_POINT('Ctrl Pts',(7.567676316871,3.30321853515081,339.911366338648));
#17343=CARTESIAN_POINT('Ctrl Pts',(7.56027906903066,3.43161352860415,339.819954268746));
#17344=CARTESIAN_POINT('Ctrl Pts',(7.55288068383599,3.56002826326455,339.728528143898));
#17345=CARTESIAN_POINT('Ctrl Pts',(7.54548229864138,3.68476407766208,339.631982746917));
#17346=CARTESIAN_POINT('Ctrl Pts',(7.53808391344671,3.80540041739779,339.530657593084));
#17347=CARTESIAN_POINT('Ctrl Pts',(7.5306829308802,3.92607910927172,339.429296866745));
#17348=CARTESIAN_POINT('Ctrl Pts',(7.52328194831367,4.04265517541928,339.323153282448));
#17349=CARTESIAN_POINT('Ctrl Pts',(7.51588096574716,4.15474302842909,339.212605005246));
#17350=CARTESIAN_POINT('Ctrl Pts',(7.50847185950113,4.2669539145344,339.101935384861));
#17351=CARTESIAN_POINT('Ctrl Pts',(7.50106275325512,4.37466648318501,338.986851678421));
#17352=CARTESIAN_POINT('Ctrl Pts',(7.4936536470091,4.47753325759919,338.867767636453));
#17353=CARTESIAN_POINT('Ctrl Pts',(7.48623997820027,4.58046337786138,338.748610261967));
#17354=CARTESIAN_POINT('Ctrl Pts',(7.47882630939142,4.67854152580117,338.625447934506));
#17355=CARTESIAN_POINT('Ctrl Pts',(7.4714126405826,4.7714623984152,338.498725073939));
#17356=CARTESIAN_POINT('Ctrl Pts',(7.46398842071034,4.8645155151376,338.371821862594));
#17357=CARTESIAN_POINT('Ctrl Pts',(7.45656420083807,4.95239648958604,338.241348306394));
#17358=CARTESIAN_POINT('Ctrl Pts',(7.44913998096581,5.03484454188067,338.107775893078));
#17359=CARTESIAN_POINT('Ctrl Pts',(7.44528429112804,5.07766306326687,338.0384064771));
#17360=CARTESIAN_POINT('Ctrl Pts',(7.44142860129029,5.11901702152002,337.968201640311));
#17361=CARTESIAN_POINT('Ctrl Pts',(7.43757291145252,5.15887497375226,337.897229636686));
#17362=CARTESIAN_POINT('Ctrl Pts',(7.43014849024341,5.23562446304105,337.760567697803));
#17363=CARTESIAN_POINT('Ctrl Pts',(7.42272406903432,5.30705548352638,337.620647962498));
#17364=CARTESIAN_POINT('Ctrl Pts',(7.41529964782521,5.37287886999374,337.477923164845));
#17365=CARTESIAN_POINT('Ctrl Pts',(7.40788398540425,5.4386246028526,337.335366743451));
#17366=CARTESIAN_POINT('Ctrl Pts',(7.40046832298325,5.49877571517569,337.190012182323));
#17367=CARTESIAN_POINT('Ctrl Pts',(7.39305266056229,5.55308761983282,337.042338965245));
#17368=CARTESIAN_POINT('Ctrl Pts',(7.38564413085279,5.60734728490267,336.894807786786));
#17369=CARTESIAN_POINT('Ctrl Pts',(7.37823560114328,5.65577879560776,336.744962740159));
#17370=CARTESIAN_POINT('Ctrl Pts',(7.37082707143378,5.69818464721681,336.593305459955));
#17371=CARTESIAN_POINT('Ctrl Pts',(7.36342405396734,5.74055894717253,336.441761018846));
#17372=CARTESIAN_POINT('Ctrl Pts',(7.35602103650091,5.77691641496336,336.288407386816));
#17373=CARTESIAN_POINT('Ctrl Pts',(7.34861801903446,5.80710864800857,336.133763517108));
#17374=CARTESIAN_POINT('Ctrl Pts',(7.34121889770174,5.8372849911848,335.979201034915));
#17375=CARTESIAN_POINT('Ctrl Pts',(7.33381977636903,5.86130249032085,335.823350032718));
#17376=CARTESIAN_POINT('Ctrl Pts',(7.32642065503632,5.87906335880463,335.666741768349));
#17377=CARTESIAN_POINT('Ctrl Pts',(7.31902275378596,5.89682129859981,335.510159327989));
#17378=CARTESIAN_POINT('Ctrl Pts',(7.31162485253557,5.90832461331464,335.352820243706));
#17379=CARTESIAN_POINT('Ctrl Pts',(7.30422695128522,5.91352710806851,335.195263167645));
#17380=CARTESIAN_POINT('Ctrl Pts',(7.29682937053205,5.91872937743618,335.037712917385));
#17381=CARTESIAN_POINT('Ctrl Pts',(7.28943178977891,5.9176313572819,334.879945067081));
#17382=CARTESIAN_POINT('Ctrl Pts',(7.28203420902574,5.91023895237013,334.722500291195));
#17383=CARTESIAN_POINT('Ctrl Pts',(7.27463548944905,5.90284540943165,334.56503127741));
#17384=CARTESIAN_POINT('Ctrl Pts',(7.26723676987232,5.88915556984469,334.407885809846));
#17385=CARTESIAN_POINT('Ctrl Pts',(7.25983805029563,5.86922737377835,334.251601311204));
#17386=CARTESIAN_POINT('Ctrl Pts',(7.25243673217286,5.84929217861774,334.095261923001));
#17387=CARTESIAN_POINT('Ctrl Pts',(7.24503541405014,5.8231143118444,333.939784475702));
#17388=CARTESIAN_POINT('Ctrl Pts',(7.23763409592738,5.79080313744415,333.785697901728));
#17389=CARTESIAN_POINT('Ctrl Pts',(7.23022465405535,5.7584564980261,333.63144220103));
#17390=CARTESIAN_POINT('Ctrl Pts',(7.22281521218332,5.7199631834998,333.478580787866));
#17391=CARTESIAN_POINT('Ctrl Pts',(7.21540577031129,5.6754831059991,333.327629802939));
#17392=CARTESIAN_POINT('Ctrl Pts',(7.20799176533832,5.63097563546562,333.176585854926));
#17393=CARTESIAN_POINT('Ctrl Pts',(7.20057776036531,5.58047417462009,333.027455032182));
#17394=CARTESIAN_POINT('Ctrl Pts',(7.19316375539233,5.52418724856345,332.880734607155));
#17395=CARTESIAN_POINT('Ctrl Pts',(7.18573920142785,5.46782023484748,332.733805421476));
#17396=CARTESIAN_POINT('Ctrl Pts',(7.17831464746342,5.40565146237075,332.589293825029));
#17397=CARTESIAN_POINT('Ctrl Pts',(7.17089009349894,5.33793631198391,332.447674297488));
#17398=CARTESIAN_POINT('Ctrl Pts',(7.1670383547255,5.30280678480394,332.374204372168));
#17399=CARTESIAN_POINT('Ctrl Pts',(7.16318661595206,5.26618526045492,332.301512369746));
#17400=CARTESIAN_POINT('Ctrl Pts',(7.15933487717862,5.22811199131594,332.229661470369));
#17401=CARTESIAN_POINT('Ctrl Pts',(7.15191226308202,5.15474170302862,332.091198939563));
#17402=CARTESIAN_POINT('Ctrl Pts',(7.14448964898538,5.0757560925081,331.955443846164));
#17403=CARTESIAN_POINT('Ctrl Pts',(7.13706703488879,4.9913791561326,331.822884219575));
#17404=CARTESIAN_POINT('Ctrl Pts',(7.12965318375392,4.90710183316211,331.69048108973));
#17405=CARTESIAN_POINT('Ctrl Pts',(7.122239332619,4.81744605215242,331.561266229439));
#17406=CARTESIAN_POINT('Ctrl Pts',(7.11482548148413,4.7226824349692,331.435704672599));
#17407=CARTESIAN_POINT('Ctrl Pts',(7.10741876549543,4.6280100190048,331.310263957147));
#17408=CARTESIAN_POINT('Ctrl Pts',(7.1000120495068,4.5282397766885,331.188469841576));
#17409=CARTESIAN_POINT('Ctrl Pts',(7.09260533351809,4.42368644346961,331.070759766524));
#17410=CARTESIAN_POINT('Ctrl Pts',(7.08520413048362,4.31921093120953,330.953137305235));
#17411=CARTESIAN_POINT('Ctrl Pts',(7.07780292744912,4.20995966364025,330.839593109715));
#17412=CARTESIAN_POINT('Ctrl Pts',(7.07040172441464,4.0962885189564,330.730532710985));
#17413=CARTESIAN_POINT('Ctrl Pts',(7.06300441651111,3.98267719751919,330.621529708942));
#17414=CARTESIAN_POINT('Ctrl Pts',(7.05560710860761,3.86465090025415,330.517006061975));
#17415=CARTESIAN_POINT('Ctrl Pts',(7.04820980070409,3.74260324997276,330.41733140236));
#17416=CARTESIAN_POINT('Ctrl Pts',(7.04081370563754,3.62057561020136,330.317673085058));
#17417=CARTESIAN_POINT('Ctrl Pts',(7.033417610571,3.49452821479502,330.222862413263));
#17418=CARTESIAN_POINT('Ctrl Pts',(7.02602151550445,3.36488882944026,330.133229640921));
#17419=CARTESIAN_POINT('Ctrl Pts',(7.01862573626671,3.23525497995955,330.043600696087));
#17420=CARTESIAN_POINT('Ctrl Pts',(7.01122995702894,3.10202975260531,329.959149423422));
#17421=CARTESIAN_POINT('Ctrl Pts',(7.00383417779119,2.96567081092048,329.880163361615));
#17422=CARTESIAN_POINT('Ctrl Pts',(6.9964372535232,2.82929075785482,329.801165071017));
#17423=CARTESIAN_POINT('Ctrl Pts',(6.9890403292552,2.68977634752289,329.72763386319));
#17424=CARTESIAN_POINT('Ctrl Pts',(6.98164340498721,2.54761066928102,329.659811759847));
#17425=CARTESIAN_POINT('Ctrl Pts',(6.9742438744223,2.40539489914216,329.591965759472));
#17426=CARTESIAN_POINT('Ctrl Pts',(6.96684434385742,2.26052633793631,329.5298330293));
#17427=CARTESIAN_POINT('Ctrl Pts',(6.95944481329252,2.11350876220303,329.473607752377));
#17428=CARTESIAN_POINT('Ctrl Pts',(6.95203713822121,1.96632936734119,329.417320589483));
#17429=CARTESIAN_POINT('Ctrl Pts',(6.94462946314989,1.81699658311566,329.366953998521));
#17430=CARTESIAN_POINT('Ctrl Pts',(6.93722178807857,1.66603078181876,329.322652732435));
#17431=CARTESIAN_POINT('Ctrl Pts',(6.92980954078437,1.51497180023448,329.278324122376));
#17432=CARTESIAN_POINT('Ctrl Pts',(6.9223972934902,1.36227815445302,329.240068387432));
#17433=CARTESIAN_POINT('Ctrl Pts',(6.91498504619599,1.20848065000577,329.207979188482));
#17434=CARTESIAN_POINT('Ctrl Pts',(6.90756222056022,1.05446365442841,329.175844193635));
#17435=CARTESIAN_POINT('Ctrl Pts',(6.90013939492441,0.899340021115722,329.149893372611));
#17436=CARTESIAN_POINT('Ctrl Pts',(6.89271656928864,0.74364673873536,329.130168648891));
#17437=CARTESIAN_POINT('Ctrl Pts',(6.88884332716065,0.66240573834677,329.119876256933));
#17438=CARTESIAN_POINT('Ctrl Pts',(6.88497008503266,0.581009665556887,329.111278224026));
#17439=CARTESIAN_POINT('Ctrl Pts',(6.88109684290467,0.499534715108384,329.104374873612));
#17440=CARTESIAN_POINT('Ctrl Pts',(6.87367165959166,0.34334348757668,329.09114083334));
#17441=CARTESIAN_POINT('Ctrl Pts',(6.86624647627868,0.186390603730519,329.084098033159));
#17442=CARTESIAN_POINT('Ctrl Pts',(6.85882129296567,0.0292079906773089,
329.083322092949));
#17443=CARTESIAN_POINT('Ctrl Pts',(6.85140487722359,-0.127789022956951,
329.082547068961));
#17444=CARTESIAN_POINT('Ctrl Pts',(6.84398846148152,-0.285014856387427,
329.088024177195));
#17445=CARTESIAN_POINT('Ctrl Pts',(6.83657204573944,-0.441931705204789,
329.099777382977));
#17446=CARTESIAN_POINT('Ctrl Pts',(6.82916277208321,-0.598697441457273,
329.111519270298));
#17447=CARTESIAN_POINT('Ctrl Pts',(6.82175349842697,-0.755154415918136,
329.129525195049));
#17448=CARTESIAN_POINT('Ctrl Pts',(6.81434422477074,-0.910764169096375,
329.153767094035));
#17449=CARTESIAN_POINT('Ctrl Pts',(6.80694047332627,-1.06625794464312,329.177990925272));
#17450=CARTESIAN_POINT('Ctrl Pts',(6.7995367218818,-1.22090538914842,329.208441419188));
#17451=CARTESIAN_POINT('Ctrl Pts',(6.79213297043734,-1.37417262180029,329.245038647567));
#17452=CARTESIAN_POINT('Ctrl Pts',(6.78473312569383,-1.52735898068852,329.281616564868));
#17453=CARTESIAN_POINT('Ctrl Pts',(6.77733328095034,-1.67916621619237,329.324334670712));
#17454=CARTESIAN_POINT('Ctrl Pts',(6.76993343620683,-1.82907021593176,329.373061870991));
#17455=CARTESIAN_POINT('Ctrl Pts',(6.76253482950683,-1.9789491357295,329.421780918884));
#17456=CARTESIAN_POINT('Ctrl Pts',(6.75513622280677,-2.12692509732166,329.4765069505));
#17457=CARTESIAN_POINT('Ctrl Pts',(6.74773761610678,-2.2724886305767,329.53705885201));
#17458=CARTESIAN_POINT('Ctrl Pts',(6.74033934110337,-2.41804563788316,329.597608038839));
#17459=CARTESIAN_POINT('Ctrl Pts',(6.73294106610005,-2.56119008744361,329.663982432911));
#17460=CARTESIAN_POINT('Ctrl Pts',(6.72554279109664,-2.70143224873621,329.735952662828));
#17461=CARTESIAN_POINT('Ctrl Pts',(6.71814338902837,-2.84169577474058,329.807933856803));
#17462=CARTESIAN_POINT('Ctrl Pts',(6.71074398696007,-2.97905580016819,329.885512413671));
#17463=CARTESIAN_POINT('Ctrl Pts',(6.70334458489179,-3.11304710699253,329.968412946977));
#17464=CARTESIAN_POINT('Ctrl Pts',(6.69594259660327,-3.24708524611863,330.051342455468));
#17465=CARTESIAN_POINT('Ctrl Pts',(6.68854060831471,-3.37775200530665,330.139597447738));
#17466=CARTESIAN_POINT('Ctrl Pts',(6.68113862002619,-3.50461119295173,330.232859248067));
#17467=CARTESIAN_POINT('Ctrl Pts',(6.67372852998265,-3.63160923275648,330.326223126951));
#17468=CARTESIAN_POINT('Ctrl Pts',(6.66631843993913,-3.75479107744746,330.424604536922));
#17469=CARTESIAN_POINT('Ctrl Pts',(6.6589083498956,-3.87375311502474,330.527644092166));
#17470=CARTESIAN_POINT('Ctrl Pts',(6.65149370824658,-3.99278822435404,330.630746938868));
#17471=CARTESIAN_POINT('Ctrl Pts',(6.64407906659752,-4.10759809023561,330.73851337755));
#17472=CARTESIAN_POINT('Ctrl Pts',(6.63666442494849,-4.21781640714295,330.850547588159));
#17473=CARTESIAN_POINT('Ctrl Pts',(6.62923925762629,-4.32819118771191,330.962740840235));
#17474=CARTESIAN_POINT('Ctrl Pts',(6.6218140903041,-4.43396115124822,331.079213688722));
#17475=CARTESIAN_POINT('Ctrl Pts',(6.6143889229819,-4.53480014405338,331.199537105037));
#17476=CARTESIAN_POINT('Ctrl Pts',(6.61054555153154,-4.58699583058992,331.261818204304));
#17477=CARTESIAN_POINT('Ctrl Pts',(6.60670218008119,-4.63787109250377,331.325130477312));
#17478=CARTESIAN_POINT('Ctrl Pts',(6.60285880863083,-4.68738535868419,331.389411535263));
#17479=CARTESIAN_POINT('Ctrl Pts',(6.59524185846718,-4.78551474918296,331.516806355463));
#17480=CARTESIAN_POINT('Ctrl Pts',(6.58762490830355,-4.87860233446218,331.648406409801));
#17481=CARTESIAN_POINT('Ctrl Pts',(6.58000795813993,-4.96626841017571,331.783774162067));
#17482=CARTESIAN_POINT('Ctrl Pts',(6.57258433273256,-5.05170944537365,331.915706164176));
#17483=CARTESIAN_POINT('Ctrl Pts',(6.56516070732519,-5.13200058453951,332.051216610025));
#17484=CARTESIAN_POINT('Ctrl Pts',(6.55773708191782,-5.20682964581119,332.189865554462));
#17485=CARTESIAN_POINT('Ctrl Pts',(6.55032058432585,-5.28158685974334,332.328381374713));
#17486=CARTESIAN_POINT('Ctrl Pts',(6.5429040867338,-5.35089225899854,332.470029371125));
#17487=CARTESIAN_POINT('Ctrl Pts',(6.53548758914184,-5.41447694055085,332.614340757203));
#17488=CARTESIAN_POINT('Ctrl Pts',(6.52807676346715,-5.47801299442558,332.758541778215));
#17489=CARTESIAN_POINT('Ctrl Pts',(6.52066593779253,-5.53583689122712,332.905401795468));
#17490=CARTESIAN_POINT('Ctrl Pts',(6.51325511211783,-5.58772573229615,333.054427666948));
#17491=CARTESIAN_POINT('Ctrl Pts',(6.5054881865,-5.642107900582,333.210614428009));
#17492=CARTESIAN_POINT('Ctrl Pts',(6.49772126088217,-5.68997032163118,333.369179972477));
#17493=CARTESIAN_POINT('Ctrl Pts',(6.48995433526434,-5.73111297915293,333.529532529199));
#17494=CARTESIAN_POINT('Ctrl Pts',(6.48255018059142,-5.77033398047769,333.68239547531));
#17495=CARTESIAN_POINT('Ctrl Pts',(6.4751460259185,-5.80344857707382,333.836881893236));
#17496=CARTESIAN_POINT('Ctrl Pts',(6.46774187124558,-5.83033456700946,333.992463698304));
#17497=CARTESIAN_POINT('Ctrl Pts',(6.46033894185855,-5.85721610768307,334.148019756721));
#17498=CARTESIAN_POINT('Ctrl Pts',(6.45293601247149,-5.87787103452298,334.304670474728));
#17499=CARTESIAN_POINT('Ctrl Pts',(6.44553308308446,-5.89222842132008,334.461878458443));
#17500=CARTESIAN_POINT('Ctrl Pts',(6.43812904123468,-5.90658796564931,334.619110066323));
#17501=CARTESIAN_POINT('Ctrl Pts',(6.43072499938494,-5.9146480485449,334.776898736988));
#17502=CARTESIAN_POINT('Ctrl Pts',(6.42332095753517,-5.91638967914874,334.934702779827));
#17503=CARTESIAN_POINT('Ctrl Pts',(6.4222313065914,-5.91664599447889,334.957926760418));
#17504=CARTESIAN_POINT('Ctrl Pts',(6.42114165564761,-5.91676555092528,334.981151072591));
#17505=CARTESIAN_POINT('Ctrl Pts',(6.42005200470385,-5.9167483832518,335.004373989846));
#17506=CARTESIAN_POINT('',(5.23189948583629,2.55396280645894,329.653827904464));
#17507=CARTESIAN_POINT('Ctrl Pts',(6.42004993338623,-5.91090779291692,335.004413773046));
#17508=CARTESIAN_POINT('Ctrl Pts',(6.38824021370975,-5.91561392752808,335.681685130669));
#17509=CARTESIAN_POINT('Ctrl Pts',(6.26368448260861,-5.49499298147518,338.328028889201));
#17510=CARTESIAN_POINT('Ctrl Pts',(6.04638274008274,-1.58837681372764,341.814009283852));
#17511=CARTESIAN_POINT('Ctrl Pts',(5.76814470580904,4.86755545747182,340.023264886511));
#17512=CARTESIAN_POINT('Ctrl Pts',(5.49665028772668,6.81546684580212,333.780002640514));
#17513=CARTESIAN_POINT('Ctrl Pts',(5.31790188106919,4.18981562870807,330.448172083406));
#17514=CARTESIAN_POINT('Ctrl Pts',(5.23189948583629,2.55396280645894,329.653827904464));
#17515=CARTESIAN_POINT('',(5.23167681249902,5.77251337094751,333.701531692827));
#17516=CARTESIAN_POINT('Origin',(5.23167681249902,0.,335.));
#17517=CARTESIAN_POINT('',(6.1683016202946,-5.91085010084463,335.003787828726));
#17518=CARTESIAN_POINT('Ctrl Pts',(5.23167681249901,5.7725133709475,333.701531692827));
#17519=CARTESIAN_POINT('Ctrl Pts',(5.27804981821134,5.98870477377988,334.662639296794));
#17520=CARTESIAN_POINT('Ctrl Pts',(5.37079582963592,5.92269951237704,336.683589130316));
#17521=CARTESIAN_POINT('Ctrl Pts',(5.55628785248541,3.9027738141709,340.231641120345));
#17522=CARTESIAN_POINT('Ctrl Pts',(5.78815288104678,-1.42257678303753,341.849708232943));
#17523=CARTESIAN_POINT('Ctrl Pts',(6.00761513888745,-5.45702824590155,338.421060314205));
#17524=CARTESIAN_POINT('Ctrl Pts',(6.13433138530335,-5.9154777532734,335.72734314963));
#17525=CARTESIAN_POINT('Ctrl Pts',(6.1683016202946,-5.91085010084463,335.003787828726));
#17526=CARTESIAN_POINT('',(7.91830163717014,-5.91374138950514,334.995600164335));
#17527=CARTESIAN_POINT('Ctrl Pts',(6.1683016202946,-5.91085010084463,335.003787828726));
#17528=CARTESIAN_POINT('Ctrl Pts',(6.227077396728,-5.90284327178869,333.751882277009));
#17529=CARTESIAN_POINT('Ctrl Pts',(6.37859918458608,-4.89799509763915,330.513552613149));
#17530=CARTESIAN_POINT('Ctrl Pts',(6.62286698386865,0.427294553030382,328.016370371526));
#17531=CARTESIAN_POINT('Ctrl Pts',(6.90110501814268,6.10500479148874,331.581181890746));
#17532=CARTESIAN_POINT('Ctrl Pts',(7.17934305241665,6.17814947180328,338.283125900322));
#17533=CARTESIAN_POINT('Ctrl Pts',(7.45758108669047,0.582805599993459,341.972334889221));
#17534=CARTESIAN_POINT('Ctrl Pts',(7.70390060931647,-4.84465710169942,339.573858972125));
#17535=CARTESIAN_POINT('Ctrl Pts',(7.85747412051787,-5.90181156470676,336.290745442971));
#17536=CARTESIAN_POINT('Ctrl Pts',(7.91830162029457,-5.91069881207897,334.995602787516));
#17537=CARTESIAN_POINT('',(9.66830162029456,-5.92110347897511,334.998042942288));
#17538=CARTESIAN_POINT('Ctrl Pts',(7.91830165384826,-5.91674836216028,334.995597571852));
#17539=CARTESIAN_POINT('Ctrl Pts',(7.92683772418695,-5.91661299085589,334.813662077034));
#17540=CARTESIAN_POINT('Ctrl Pts',(7.93537379452558,-5.9080821444984,334.632067955286));
#17541=CARTESIAN_POINT('Ctrl Pts',(7.94390986486428,-5.89127375261271,334.451525630246));
#17542=CARTESIAN_POINT('Ctrl Pts',(7.95248902433919,-5.87438051382923,334.270071947577));
#17543=CARTESIAN_POINT('Ctrl Pts',(7.96106818381414,-5.84912605575822,334.089680827836));
#17544=CARTESIAN_POINT('Ctrl Pts',(7.96964734328904,-5.81567951179891,333.911054464841));
#17545=CARTESIAN_POINT('Ctrl Pts',(7.97828197365068,-5.78201671012143,333.73127314456));
#17546=CARTESIAN_POINT('Ctrl Pts',(7.98691660401228,-5.74005562372791,333.553279595535));
#17547=CARTESIAN_POINT('Ctrl Pts',(7.99555123437392,-5.69001722684064,333.377768659914));
#17548=CARTESIAN_POINT('Ctrl Pts',(8.00171987466208,-5.65426944632587,333.25238242065));
#17549=CARTESIAN_POINT('Ctrl Pts',(8.00788851495028,-5.61440020520827,333.128262813615));
#17550=CARTESIAN_POINT('Ctrl Pts',(8.01405715523845,-5.57050476081265,333.005656180027));
#17551=CARTESIAN_POINT('Ctrl Pts',(8.02148123988807,-5.51767569643178,332.858096590905));
#17552=CARTESIAN_POINT('Ctrl Pts',(8.02890532453766,-5.45889976275216,332.712415060664));
#17553=CARTESIAN_POINT('Ctrl Pts',(8.03632940918729,-5.39432904919198,332.569126767694));
#17554=CARTESIAN_POINT('Ctrl Pts',(8.04374473498362,-5.32983451544838,332.426007524673));
#17555=CARTESIAN_POINT('Ctrl Pts',(8.05116006077994,-5.25955896206744,332.285276235607));
#17556=CARTESIAN_POINT('Ctrl Pts',(8.05857538657628,-5.18370390865521,332.147431972784));
#17557=CARTESIAN_POINT('Ctrl Pts',(8.06598357992732,-5.10792181657112,332.009720295729));
#17558=CARTESIAN_POINT('Ctrl Pts',(8.07339177327832,-5.02657108719275,331.874890441416));
#17559=CARTESIAN_POINT('Ctrl Pts',(8.08079996662937,-4.93990084107574,331.743420468829));
#17560=CARTESIAN_POINT('Ctrl Pts',(8.08820264833253,-4.85329507706065,331.612048309051));
#17561=CARTESIAN_POINT('Ctrl Pts',(8.09560533003574,-4.76137788117132,331.484031363918));
#17562=CARTESIAN_POINT('Ctrl Pts',(8.10300801173889,-4.66444365169039,331.359821984751));
#17563=CARTESIAN_POINT('Ctrl Pts',(8.11040679823126,-4.56756042794927,331.235677963211));
#17564=CARTESIAN_POINT('Ctrl Pts',(8.11780558472363,-4.46566565718142,331.115337811013));
#17565=CARTESIAN_POINT('Ctrl Pts',(8.125204371216,-4.35909622293599,330.999223740112));
#17566=CARTESIAN_POINT('Ctrl Pts',(8.13260194010405,-4.25254432662111,330.883128777884));
#17567=CARTESIAN_POINT('Ctrl Pts',(8.13999950899212,-4.14131954572892,330.771258791351));
#17568=CARTESIAN_POINT('Ctrl Pts',(8.14739707788016,-4.02579818218162,330.66400189589));
#17569=CARTESIAN_POINT('Ctrl Pts',(8.15479432784718,-3.91028179894503,330.556749624446));
#17570=CARTESIAN_POINT('Ctrl Pts',(8.16219157781416,-3.79046947484708,330.454110302568));
#17571=CARTESIAN_POINT('Ctrl Pts',(8.16958882778118,-3.66677320746662,330.35643404187));
#17572=CARTESIAN_POINT('Ctrl Pts',(8.17698721844369,-3.54305786546047,330.25874271897));
#17573=CARTESIAN_POINT('Ctrl Pts',(8.18438560910621,-3.41545768054302,330.166016212421));
#17574=CARTESIAN_POINT('Ctrl Pts',(8.19178399976872,-3.28441632199582,330.078563219312));
#17575=CARTESIAN_POINT('Ctrl Pts',(8.19918499114654,-3.15332889920535,329.991079484336));
#17576=CARTESIAN_POINT('Ctrl Pts',(8.20658598252437,-3.01879820458202,329.908873160688));
#17577=CARTESIAN_POINT('Ctrl Pts',(8.21398697390219,-2.88129522296416,329.832208556779));
#17578=CARTESIAN_POINT('Ctrl Pts',(8.22139609400086,-2.74364121788267,329.75545974994));
#17579=CARTESIAN_POINT('Ctrl Pts',(8.22880521409956,-2.60300873248182,329.68426500001));
#17580=CARTESIAN_POINT('Ctrl Pts',(8.23621433419822,-2.45989224565882,329.618842066781));
#17581=CARTESIAN_POINT('Ctrl Pts',(8.24362801973741,-2.31668757160171,329.553378820463));
#17582=CARTESIAN_POINT('Ctrl Pts',(8.25104170527654,-2.17099619069115,329.493694618884));
#17583=CARTESIAN_POINT('Ctrl Pts',(8.25845539081573,-2.02333021842649,329.439958148566));
#17584=CARTESIAN_POINT('Ctrl Pts',(8.26587963176961,-1.87545400315037,329.386145169644));
#17585=CARTESIAN_POINT('Ctrl Pts',(8.27330387272348,-1.72559793620386,329.338296947935));
#17586=CARTESIAN_POINT('Ctrl Pts',(8.28072811367736,-1.57428765481617,329.296531849621));
#17587=CARTESIAN_POINT('Ctrl Pts',(8.28458380562237,-1.4957064454012,329.274841638573));
#17588=CARTESIAN_POINT('Ctrl Pts',(8.28843949756739,-1.41673316862141,329.254791274787));
#17589=CARTESIAN_POINT('Ctrl Pts',(8.2922951895124,-1.33744215071377,329.236391837053));
#17590=CARTESIAN_POINT('Ctrl Pts',(8.29971898218592,-1.18477433227457,329.20096535252));
#17591=CARTESIAN_POINT('Ctrl Pts',(8.30714277485943,-1.03046754044259,329.171555439486));
#17592=CARTESIAN_POINT('Ctrl Pts',(8.31456656753295,-0.875037250964456,
329.14831303196));
#17593=CARTESIAN_POINT('Ctrl Pts',(8.32198159640168,-0.719790447310228,
329.125098062152));
#17594=CARTESIAN_POINT('Ctrl Pts',(8.32939662527037,-0.563423151547546,
329.108036160072));
#17595=CARTESIAN_POINT('Ctrl Pts',(8.3368116541391,-0.406464050401816,329.097227978464));
#17596=CARTESIAN_POINT('Ctrl Pts',(8.34421954592478,-0.249656024883776,
329.086430199902));
#17597=CARTESIAN_POINT('Ctrl Pts',(8.35162743771053,-0.0922576978533067,
329.081874183981));
#17598=CARTESIAN_POINT('Ctrl Pts',(8.35903532949621,0.0651941497774572,
329.083609184196));
#17599=CARTESIAN_POINT('Ctrl Pts',(8.36643770530399,0.222528757451586,329.085342892515));
#17600=CARTESIAN_POINT('Ctrl Pts',(8.37384008111172,0.379916434764904,329.093358285677));
#17601=CARTESIAN_POINT('Ctrl Pts',(8.38124245691949,0.536817511828146,329.107652630615));
#17602=CARTESIAN_POINT('Ctrl Pts',(8.38864093348939,0.693635940476877,329.121939445937));
#17603=CARTESIAN_POINT('Ctrl Pts',(8.39603941005929,0.849967908592966,329.142498592243));
#17604=CARTESIAN_POINT('Ctrl Pts',(8.40343788662918,1.00527609563477,329.169275299412));
#17605=CARTESIAN_POINT('Ctrl Pts',(8.41083514053918,1.16055861670482,329.196047581507));
#17606=CARTESIAN_POINT('Ctrl Pts',(8.4182323944492,1.3148173250386,329.229035321837));
#17607=CARTESIAN_POINT('Ctrl Pts',(8.42562964835921,1.46752223760303,329.268132150456));
#17608=CARTESIAN_POINT('Ctrl Pts',(8.43302658023806,1.62022050233054,329.307227277038));
#17609=CARTESIAN_POINT('Ctrl Pts',(8.44042351211688,1.77136474421501,329.352430870534));
#17610=CARTESIAN_POINT('Ctrl Pts',(8.44782044399574,1.92043761810329,329.403585976943));
#17611=CARTESIAN_POINT('Ctrl Pts',(8.45521851372274,2.06953342343079,329.454748952389));
#17612=CARTESIAN_POINT('Ctrl Pts',(8.46261658344977,2.21655687327633,329.511865142484));
#17613=CARTESIAN_POINT('Ctrl Pts',(8.47001465317678,2.36100830668288,329.574728547043));
#17614=CARTESIAN_POINT('Ctrl Pts',(8.47741532103311,2.50551047001213,329.63761402861));
#17615=CARTESIAN_POINT('Ctrl Pts',(8.48481598888946,2.6474384764872,329.706250594357));
#17616=CARTESIAN_POINT('Ctrl Pts',(8.4922166567458,2.78631520828013,329.780385251515));
#17617=CARTESIAN_POINT('Ctrl Pts',(8.49962545099421,2.92534443533359,329.854601313121));
#17618=CARTESIAN_POINT('Ctrl Pts',(8.50703424524264,3.06131536714769,329.934327346968));
#17619=CARTESIAN_POINT('Ctrl Pts',(8.51444303949106,3.19377731392234,330.019265412454));
#17620=CARTESIAN_POINT('Ctrl Pts',(8.52185639737291,3.32632085396972,330.104255797682));
#17621=CARTESIAN_POINT('Ctrl Pts',(8.52926975525478,3.45535079683766,330.194464398494));
#17622=CARTESIAN_POINT('Ctrl Pts',(8.53668311313663,3.58044817403435,330.289551885908));
#17623=CARTESIAN_POINT('Ctrl Pts',(8.54410702640874,3.70572366911725,330.384774762109));
#17624=CARTESIAN_POINT('Ctrl Pts',(8.55153093968082,3.82705512846242,330.484890162004));
#17625=CARTESIAN_POINT('Ctrl Pts',(8.55895485295292,3.94405858059623,330.58952015362));
#17626=CARTESIAN_POINT('Ctrl Pts',(8.56281430989739,4.00488496276339,330.643913966282));
#17627=CARTESIAN_POINT('Ctrl Pts',(8.56667376684183,4.06454227385321,330.699527320161));
#17628=CARTESIAN_POINT('Ctrl Pts',(8.5705332237863,4.12298082739577,330.756303538255));
#17629=CARTESIAN_POINT('Ctrl Pts',(8.57795727706771,4.23539325780528,330.865518299376));
#17630=CARTESIAN_POINT('Ctrl Pts',(8.58538133034913,4.34363271208492,330.979367457087));
#17631=CARTESIAN_POINT('Ctrl Pts',(8.59280538363055,4.44729331096703,331.097499164801));
#17632=CARTESIAN_POINT('Ctrl Pts',(8.60022067615752,4.55083158515432,331.215491471188));
#17633=CARTESIAN_POINT('Ctrl Pts',(8.60763596868448,4.64980151550148,331.337755990468));
#17634=CARTESIAN_POINT('Ctrl Pts',(8.61505126121145,4.74383235924362,331.463902559333));
#17635=CARTESIAN_POINT('Ctrl Pts',(8.62245941943236,4.8377727352374,331.58992776168));
#17636=CARTESIAN_POINT('Ctrl Pts',(8.62986757765331,4.92678326328722,331.719827280803));
#17637=CARTESIAN_POINT('Ctrl Pts',(8.63727573587423,5.01053204567707,331.853176334501));
#17638=CARTESIAN_POINT('Ctrl Pts',(8.64467838062512,5.09421849862048,331.986426144098));
#17639=CARTESIAN_POINT('Ctrl Pts',(8.65208102537597,5.17265080563063,332.123120061727));
#17640=CARTESIAN_POINT('Ctrl Pts',(8.65948367012686,5.24553922421881,332.262802745566));
#17641=CARTESIAN_POINT('Ctrl Pts',(8.66688241788194,5.31838927194478,332.402411895843));
#17642=CARTESIAN_POINT('Ctrl Pts',(8.67428116563706,5.38570107137234,332.545006348807));
#17643=CARTESIAN_POINT('Ctrl Pts',(8.68167991339214,5.44722991195677,332.690104580553));
#17644=CARTESIAN_POINT('Ctrl Pts',(8.68907744097947,5.50874860548524,332.835178883359));
#17645=CARTESIAN_POINT('Ctrl Pts',(8.69647496856678,5.56448608739801,332.982755802199));
#17646=CARTESIAN_POINT('Ctrl Pts',(8.7038724961541,5.61424501031915,333.132332062007));
#17647=CARTESIAN_POINT('Ctrl Pts',(8.71126970323063,5.66400177734807,333.281901841163));
#17648=CARTESIAN_POINT('Ctrl Pts',(8.71866691030714,5.70778038262102,333.433470434927));
#17649=CARTESIAN_POINT('Ctrl Pts',(8.72606411738366,5.74543285576739,333.586517823823));
#17650=CARTESIAN_POINT('Ctrl Pts',(8.73346246359525,5.78309112721737,333.739588781298));
#17651=CARTESIAN_POINT('Ctrl Pts',(8.74086080980685,5.81462129895377,333.894138624922));
#17652=CARTESIAN_POINT('Ctrl Pts',(8.74825915601843,5.83992621491512,334.049635666259));
#17653=CARTESIAN_POINT('Ctrl Pts',(8.75566010141336,5.86524002098702,334.205187336739));
#17654=CARTESIAN_POINT('Ctrl Pts',(8.76306104680832,5.88432415695462,334.361686499351));
#17655=CARTESIAN_POINT('Ctrl Pts',(8.77046199220325,5.89713318336375,334.518594993618));
#17656=CARTESIAN_POINT('Ctrl Pts',(8.77787106420263,5.90995627471803,334.675675781179));
#17657=CARTESIAN_POINT('Ctrl Pts',(8.78528013620195,5.91649046567086,334.833166425817));
#17658=CARTESIAN_POINT('Ctrl Pts',(8.79268920820132,5.91674241610059,334.990526668159));
#17659=CARTESIAN_POINT('Ctrl Pts',(8.8001028443691,5.9169945217379,335.147983848234));
#17660=CARTESIAN_POINT('Ctrl Pts',(8.80751648053688,5.91095668961467,335.305310093885));
#17661=CARTESIAN_POINT('Ctrl Pts',(8.81493011670466,5.89868755012404,335.461969423784));
#17662=CARTESIAN_POINT('Ctrl Pts',(8.82235430671008,5.8864009446419,335.618851769367));
#17663=CARTESIAN_POINT('Ctrl Pts',(8.82977849671553,5.86786535906686,335.775064933449));
#17664=CARTESIAN_POINT('Ctrl Pts',(8.83720268672096,5.84319082462592,335.930081474661));
#17665=CARTESIAN_POINT('Ctrl Pts',(8.84105887716739,5.83037465156034,336.010598447533));
#17666=CARTESIAN_POINT('Ctrl Pts',(8.84491506761377,5.81590311068985,336.090792800601));
#17667=CARTESIAN_POINT('Ctrl Pts',(8.8487712580602,5.79979691940674,336.170592267248));
#17668=CARTESIAN_POINT('Ctrl Pts',(8.85619524385121,5.7687890797022,336.324223192573));
#17669=CARTESIAN_POINT('Ctrl Pts',(8.86361922964221,5.73162595104128,336.476852966426));
#17670=CARTESIAN_POINT('Ctrl Pts',(8.87104321543322,5.68838375572378,336.627949879486));
#17671=CARTESIAN_POINT('Ctrl Pts',(8.87845844010974,5.64519259092201,336.778868481677));
#17672=CARTESIAN_POINT('Ctrl Pts',(8.88587366478632,5.59593674103953,336.928257468488));
#17673=CARTESIAN_POINT('Ctrl Pts',(8.89328888946284,5.54074366422659,337.075593941462));
#17674=CARTESIAN_POINT('Ctrl Pts',(8.90069697954199,5.4856036917224,337.222788653874));
#17675=CARTESIAN_POINT('Ctrl Pts',(8.9081050696211,5.42453799492601,337.367934436824));
#17676=CARTESIAN_POINT('Ctrl Pts',(8.91551315970025,5.35772416521539,337.510522322539));
#17677=CARTESIAN_POINT('Ctrl Pts',(8.92291573608602,5.29096006370282,337.653004082941));
#17678=CARTESIAN_POINT('Ctrl Pts',(8.9303183124718,5.21845650551427,337.792931400333));
#17679=CARTESIAN_POINT('Ctrl Pts',(8.93772088885757,5.14043959309047,337.92981421805));
#17680=CARTESIAN_POINT('Ctrl Pts',(8.94511956809161,5.06246375335933,338.066624972599));
#17681=CARTESIAN_POINT('Ctrl Pts',(8.9525182473257,4.97898052434013,338.200394096124));
#17682=CARTESIAN_POINT('Ctrl Pts',(8.95991692655974,4.89026239513531,338.330655231216));
#17683=CARTESIAN_POINT('Ctrl Pts',(8.96731438561524,4.80155889718485,338.460894883846));
#17684=CARTESIAN_POINT('Ctrl Pts',(8.97471184467069,4.70762242236363,338.587627388077));
#17685=CARTESIAN_POINT('Ctrl Pts',(8.98210930372619,4.60876938193421,338.710414444054));
#17686=CARTESIAN_POINT('Ctrl Pts',(8.9895064422716,4.50992062451558,338.833196180031));
#17687=CARTESIAN_POINT('Ctrl Pts',(8.99690358081701,4.40615595908437,338.952032516941));
#17688=CARTESIAN_POINT('Ctrl Pts',(9.00430071936242,4.29783259854894,339.066517615522));
#17689=CARTESIAN_POINT('Ctrl Pts',(9.01169899710373,4.18949255568047,339.181020345374));
#17690=CARTESIAN_POINT('Ctrl Pts',(9.01909727484511,4.07659267632957,339.291170231504));
#17691=CARTESIAN_POINT('Ctrl Pts',(9.02649555258643,3.95952748475246,339.39659785061));
#17692=CARTESIAN_POINT('Ctrl Pts',(9.03389642963216,3.84242116359358,339.502062510564));
#17693=CARTESIAN_POINT('Ctrl Pts',(9.04129730667785,3.72114689365642,339.602801350596));
#17694=CARTESIAN_POINT('Ctrl Pts',(9.04869818372359,3.59613262855752,339.698484934564));
#17695=CARTESIAN_POINT('Ctrl Pts',(9.05610718790516,3.47098108136252,339.794273591684));
#17696=CARTESIAN_POINT('Ctrl Pts',(9.06351619208672,3.34208163363746,339.884995679458));
#17697=CARTESIAN_POINT('Ctrl Pts',(9.07092519626829,3.20989219798347,339.970364437325));
#17698=CARTESIAN_POINT('Ctrl Pts',(9.07833876481848,3.07762132610715,340.05578578721));
#17699=CARTESIAN_POINT('Ctrl Pts',(9.08575233336862,2.94205674819764,340.135847046234));
#17700=CARTESIAN_POINT('Ctrl Pts',(9.09316590191881,2.80368090346349,340.210307472122));
#17701=CARTESIAN_POINT('Ctrl Pts',(9.1005900252035,2.66510805234929,340.28487390769));
#17702=CARTESIAN_POINT('Ctrl Pts',(9.10801414848822,2.5237162753334,340.353823421439));
#17703=CARTESIAN_POINT('Ctrl Pts',(9.11543827177292,2.38000864603019,340.416963116666));
#17704=CARTESIAN_POINT('Ctrl Pts',(9.11929527862669,2.3053491488873,340.449765675015));
#17705=CARTESIAN_POINT('Ctrl Pts',(9.12315228548043,2.23006486464686,340.481000950716));
#17706=CARTESIAN_POINT('Ctrl Pts',(9.12700929233421,2.15422782191943,340.510647244541));
#17707=CARTESIAN_POINT('Ctrl Pts',(9.13443324371234,2.0082569851502,340.567710312417));
#17708=CARTESIAN_POINT('Ctrl Pts',(9.14185719509051,1.85979705777193,340.619055559184));
#17709=CARTESIAN_POINT('Ctrl Pts',(9.14928114646864,1.70933640674325,340.664459339697));
#17710=CARTESIAN_POINT('Ctrl Pts',(9.15669633608286,1.5590533297093,340.709809534568));
#17711=CARTESIAN_POINT('Ctrl Pts',(9.16411152569702,1.40677458297222,340.74923211417));
#17712=CARTESIAN_POINT('Ctrl Pts',(9.17152671531124,1.25300885155084,340.782551286451));
#17713=CARTESIAN_POINT('Ctrl Pts',(9.178934769716,1.09939108002805,340.815838397613));
#17714=CARTESIAN_POINT('Ctrl Pts',(9.18634282412077,0.944289534666818,340.843033714906));
#17715=CARTESIAN_POINT('Ctrl Pts',(9.19375087852552,0.788228316462973,340.864011142863));
#17716=CARTESIAN_POINT('Ctrl Pts',(9.20115341866133,0.632283264188988,340.884972956035));
#17717=CARTESIAN_POINT('Ctrl Pts',(9.20855595879715,0.475380329736878,340.899726046095));
#17718=CARTESIAN_POINT('Ctrl Pts',(9.21595849893296,0.318053964055267,340.908195345319));
#17719=CARTESIAN_POINT('Ctrl Pts',(9.22335714137742,0.160810436102888,340.916660185167));
#17720=CARTESIAN_POINT('Ctrl Pts',(9.23075578382188,0.0031442926772372,
340.918847803503));
#17721=CARTESIAN_POINT('Ctrl Pts',(9.23815442626633,-0.154404841455918,
340.914734965105));
#17722=CARTESIAN_POINT('Ctrl Pts',(9.24555184783926,-0.311927977947833,
340.910622805379));
#17723=CARTESIAN_POINT('Ctrl Pts',(9.25294926941215,-0.469333770743121,
340.900212262033));
#17724=CARTESIAN_POINT('Ctrl Pts',(9.26034669098507,-0.626082420024908,
340.883532218475));
#17725=CARTESIAN_POINT('Ctrl Pts',(9.26774379162101,-0.782824268769665,
340.866852898581));
#17726=CARTESIAN_POINT('Ctrl Pts',(9.27514089225692,-0.938908659569522,
340.843904658796));
#17727=CARTESIAN_POINT('Ctrl Pts',(9.28253799289286,-1.09380100885479,340.81476825983));
#17728=CARTESIAN_POINT('Ctrl Pts',(9.28993623232881,-1.24871720416013,340.785627375251));
#17729=CARTESIAN_POINT('Ctrl Pts',(9.29733447176483,-1.40244062573968,340.750296503577));
#17730=CARTESIAN_POINT('Ctrl Pts',(9.30473271120078,-1.55444712128882,340.708907488269));
#17731=CARTESIAN_POINT('Ctrl Pts',(9.3121335495761,-1.70650701544281,340.667503933348));
#17732=CARTESIAN_POINT('Ctrl Pts',(9.31953438795144,-1.85684842283524,340.62003809559));
#17733=CARTESIAN_POINT('Ctrl Pts',(9.32693522632675,-2.00496272635088,340.566691569365));
#17734=CARTESIAN_POINT('Ctrl Pts',(9.33434419147376,-2.15323967240338,340.513286463962));
#17735=CARTESIAN_POINT('Ctrl Pts',(9.34175315662073,-2.29928427933032,340.453987900637));
#17736=CARTESIAN_POINT('Ctrl Pts',(9.34916212176773,-2.44260760404967,340.389025761224));
#17737=CARTESIAN_POINT('Ctrl Pts',(9.35657565101858,-2.58601921944444,340.324023603544));
#17738=CARTESIAN_POINT('Ctrl Pts',(9.36398918026944,-2.72670587950936,340.25335108482));
#17739=CARTESIAN_POINT('Ctrl Pts',(9.37140270952028,-2.86420406596059,340.177283615086));
#17740=CARTESIAN_POINT('Ctrl Pts',(9.3788267934271,-3.00189800884647,340.101107847947));
#17741=CARTESIAN_POINT('Ctrl Pts',(9.38625087733393,-3.13639409372241,340.019521982744));
#17742=CARTESIAN_POINT('Ctrl Pts',(9.39367496124075,-3.26725787003449,339.932844673532));
#17743=CARTESIAN_POINT('Ctrl Pts',(9.39753241636321,-3.33525294533478,339.887808298053));
#17744=CARTESIAN_POINT('Ctrl Pts',(9.40138987148567,-3.40226794297014,339.84139805386));
#17745=CARTESIAN_POINT('Ctrl Pts',(9.40524732660813,-3.46824561639963,339.793662786098));
#17746=CARTESIAN_POINT('Ctrl Pts',(9.41261048706837,-3.59418465673371,339.702545086739));
#17747=CARTESIAN_POINT('Ctrl Pts',(9.4199736475286,-3.71673576760079,339.606312329512));
#17748=CARTESIAN_POINT('Ctrl Pts',(9.42733680798884,-3.83545069730018,339.505246775825));
#17749=CARTESIAN_POINT('Ctrl Pts',(9.43469124851353,-3.95402503702593,339.404300910568));
#17750=CARTESIAN_POINT('Ctrl Pts',(9.44204568903819,-4.0687719495888,339.298533881596));
#17751=CARTESIAN_POINT('Ctrl Pts',(9.44940012956289,-4.17927208776007,339.188271168271));
#17752=CARTESIAN_POINT('Ctrl Pts',(9.45674753057803,-4.28966645761678,339.078113996003));
#17753=CARTESIAN_POINT('Ctrl Pts',(9.46409493159318,-4.39582187617995,338.963469970323));
#17754=CARTESIAN_POINT('Ctrl Pts',(9.47144233260832,-4.49735219872133,338.844704639261));
#17755=CARTESIAN_POINT('Ctrl Pts',(9.47878436825251,-4.59880837969331,338.726026035472));
#17756=CARTESIAN_POINT('Ctrl Pts',(9.48612640389676,-4.69564594199118,338.603232404785));
#17757=CARTESIAN_POINT('Ctrl Pts',(9.49346843954095,-4.78751589011209,338.476725782173));
#17758=CARTESIAN_POINT('Ctrl Pts',(9.50080733153183,-4.87934650210338,338.35027332614));
#17759=CARTESIAN_POINT('Ctrl Pts',(9.50814622352271,-4.9662135087272,338.220111347855));
#17760=CARTESIAN_POINT('Ctrl Pts',(9.5154851155136,-5.04780854743308,338.086674493846));
#17761=CARTESIAN_POINT('Ctrl Pts',(9.52282245051373,-5.12938627525321,337.953265949281));
#17762=CARTESIAN_POINT('Ctrl Pts',(9.53015978551386,-5.20569406209302,337.816584235143));
#17763=CARTESIAN_POINT('Ctrl Pts',(9.53749712051399,-5.27646732766874,337.677092285026));
#17764=CARTESIAN_POINT('Ctrl Pts',(9.54483440613936,-5.34724011699347,337.537601273584));
#17765=CARTESIAN_POINT('Ctrl Pts',(9.55217169176475,-5.41247828707875,337.395300402612));
#17766=CARTESIAN_POINT('Ctrl Pts',(9.55950897739012,-5.47196372468579,337.250676244648));
#17767=CARTESIAN_POINT('Ctrl Pts',(9.56684772099427,-5.53146098253663,337.106023348678));
#17768=CARTESIAN_POINT('Ctrl Pts',(9.57418646459841,-5.58520308859339,336.959046598407));
#17769=CARTESIAN_POINT('Ctrl Pts',(9.58152520820255,-5.63302057482098,336.810251299169));
#17770=CARTESIAN_POINT('Ctrl Pts',(9.58887113577307,-5.68088487004367,336.661310342788));
#17771=CARTESIAN_POINT('Ctrl Pts',(9.59621706334361,-5.72281284390395,336.510547643699));
#17772=CARTESIAN_POINT('Ctrl Pts',(9.60356299091413,-5.75868512950576,336.358483029599));
#17773=CARTESIAN_POINT('Ctrl Pts',(9.61091255689113,-5.79457518249709,336.206343098547));
#17774=CARTESIAN_POINT('Ctrl Pts',(9.61826212286808,-5.82440349896535,336.052900340431));
#17775=CARTESIAN_POINT('Ctrl Pts',(9.62561168884508,-5.84810223963961,335.8986827901));
#17776=CARTESIAN_POINT('Ctrl Pts',(9.63297217355516,-5.8718361878655,335.744236129605));
#17777=CARTESIAN_POINT('Ctrl Pts',(9.64033265826531,-5.88942232263109,335.589012754514));
#17778=CARTESIAN_POINT('Ctrl Pts',(9.64769314297538,-5.90084480945455,335.433544804182));
#17779=CARTESIAN_POINT('Ctrl Pts',(9.65456263541512,-5.91150534201013,335.288447578729));
#17780=CARTESIAN_POINT('Ctrl Pts',(9.66143212785482,-5.91679763337387,335.143137580778));
#17781=CARTESIAN_POINT('Ctrl Pts',(9.66830162029456,-5.91674967681206,334.998044381317));
#17782=CARTESIAN_POINT('',(11.4183016202945,-5.91660642682179,335.005447186169));
#17783=CARTESIAN_POINT('Ctrl Pts',(9.66830162029456,-5.92571575529067,334.998041417827));
#17784=CARTESIAN_POINT('Ctrl Pts',(9.67336286715706,-5.92617653575604,334.890978712543));
#17785=CARTESIAN_POINT('Ctrl Pts',(9.67842411401957,-5.92352695970669,334.783939278396));
#17786=CARTESIAN_POINT('Ctrl Pts',(9.77623137230671,-5.81083203592888,332.718786120812));
#17787=CARTESIAN_POINT('Ctrl Pts',(9.96172339515596,-3.46005639991333,328.918829283388));
#17788=CARTESIAN_POINT('Ctrl Pts',(10.23996142943,3.24135166517253,328.799494881017));
#17789=CARTESIAN_POINT('Ctrl Pts',(10.5181994637039,6.9682181308629,334.370272377245));
#17790=CARTESIAN_POINT('Ctrl Pts',(10.7964374979778,4.30045420801287,340.518941686844));
#17791=CARTESIAN_POINT('Ctrl Pts',(11.0746755322517,-2.31377335260903,341.602959633473));
#17792=CARTESIAN_POINT('Ctrl Pts',(11.281963573024,-5.65951399291435,337.89625865298));
#17793=CARTESIAN_POINT('Ctrl Pts',(11.3965056023716,-5.92087158251783,335.468355196754));
#17794=CARTESIAN_POINT('Ctrl Pts',(11.4183016202945,-5.91660642682179,335.005447186169));
#17795=CARTESIAN_POINT('',(13.1683016202945,-5.90706551088391,334.999199780965));
#17796=CARTESIAN_POINT('Ctrl Pts',(11.4183016202945,-5.91660642682179,335.005447186169));
#17797=CARTESIAN_POINT('Ctrl Pts',(11.4892516137962,-5.90272257106488,333.498597611211));
#17798=CARTESIAN_POINT('Ctrl Pts',(11.6529476187225,-4.55055703177909,329.999836531847));
#17799=CARTESIAN_POINT('Ctrl Pts',(11.9093896350736,1.3378723248115,328.132488036437));
#17800=CARTESIAN_POINT('Ctrl Pts',(12.1876276693475,6.49903679796859,332.408640592677));
#17801=CARTESIAN_POINT('Ctrl Pts',(12.4658657036214,5.69613113915697,339.062845430127));
#17802=CARTESIAN_POINT('Ctrl Pts',(12.7441037378953,-0.334029997602265,
341.988636983051));
#17803=CARTESIAN_POINT('Ctrl Pts',(12.9782490434532,-5.15062645695485,339.053740283081));
#17804=CARTESIAN_POINT('Ctrl Pts',(13.1196483375861,-5.90581620181614,336.036722990494));
#17805=CARTESIAN_POINT('Ctrl Pts',(13.1683016202945,-5.90706551088391,334.999199780965));
#17806=CARTESIAN_POINT('',(14.9183007632462,-5.91862575758834,334.994894904104));
#17807=CARTESIAN_POINT('Ctrl Pts',(13.1683016202945,-5.90706551088391,334.999199780965));
#17808=CARTESIAN_POINT('Ctrl Pts',(13.2123943490108,-5.90819771497666,334.058929631288));
#17809=CARTESIAN_POINT('Ctrl Pts',(13.3492330891516,-5.25256836435763,331.142357715814));
#17810=CARTESIAN_POINT('Ctrl Pts',(13.5788178407172,-0.676788508317976,
328.036194988672));
#17811=CARTESIAN_POINT('Ctrl Pts',(13.8570558749913,5.48976310418741,330.662359629893));
#17812=CARTESIAN_POINT('Ctrl Pts',(14.1352939092649,6.61844014501037,337.269112815324));
#17813=CARTESIAN_POINT('Ctrl Pts',(14.4135319435389,1.67347235263872,341.793534662167));
#17814=CARTESIAN_POINT('Ctrl Pts',(14.6745340873688,-4.40575991606507,340.189552740701));
#17815=CARTESIAN_POINT('Ctrl Pts',(14.842790219774,-5.90491800172395,336.596553961129));
#17816=CARTESIAN_POINT('Ctrl Pts',(14.9183003407544,-5.91955152666098,334.994903064175));
#17817=CARTESIAN_POINT('',(16.6683030484718,-5.92081106350143,335.003451021425));
#17818=CARTESIAN_POINT('Ctrl Pts',(14.9183016202945,-5.91674778330215,334.994878350942));
#17819=CARTESIAN_POINT('Ctrl Pts',(14.9293698822705,-5.91654466019703,334.760221862702));
#17820=CARTESIAN_POINT('Ctrl Pts',(14.9404381442466,-5.90237883094342,334.526146915353));
#17821=CARTESIAN_POINT('Ctrl Pts',(14.9515064062226,-5.87447532519484,334.293975767996));
#17822=CARTESIAN_POINT('Ctrl Pts',(14.9576736081773,-5.85892757654459,334.164610709875));
#17823=CARTESIAN_POINT('Ctrl Pts',(14.9638408101321,-5.8391154726375,334.035835989689));
#17824=CARTESIAN_POINT('Ctrl Pts',(14.9700080120869,-5.81508355031101,333.907876442246));
#17825=CARTESIAN_POINT('Ctrl Pts',(14.9774319895248,-5.78615431296009,333.753840819584));
#17826=CARTESIAN_POINT('Ctrl Pts',(14.9848559669627,-5.75105683838513,333.600723079315));
#17827=CARTESIAN_POINT('Ctrl Pts',(14.9922799444006,-5.70986015551614,333.449055911082));
#17828=CARTESIAN_POINT('Ctrl Pts',(14.9996951604281,-5.6687120909313,333.297567732928));
#17829=CARTESIAN_POINT('Ctrl Pts',(15.0071103764557,-5.62147924263076,333.147527075918));
#17830=CARTESIAN_POINT('Ctrl Pts',(15.0145255924832,-5.56828198979593,332.999458512149));
#17831=CARTESIAN_POINT('Ctrl Pts',(15.0219336736272,-5.51513592308989,332.851532419206));
#17832=CARTESIAN_POINT('Ctrl Pts',(15.0293417547712,-5.45603700231441,332.705574990743));
#17833=CARTESIAN_POINT('Ctrl Pts',(15.0367498359152,-5.39115592357888,332.562097547038));
#17834=CARTESIAN_POINT('Ctrl Pts',(15.0441524030891,-5.32632313701521,332.418726896214));
#17835=CARTESIAN_POINT('Ctrl Pts',(15.051554970263,-5.25571691503302,332.277832893299));
#17836=CARTESIAN_POINT('Ctrl Pts',(15.058957537437,-5.17955671596436,332.13990860485));
#17837=CARTESIAN_POINT('Ctrl Pts',(15.0663562071916,-5.10343661490798,332.002056932937));
#17838=CARTESIAN_POINT('Ctrl Pts',(15.0737548769462,-5.02176854032462,331.867172187492));
#17839=CARTESIAN_POINT('Ctrl Pts',(15.0811535467008,-4.9348186532721,331.735724364914));
#17840=CARTESIAN_POINT('Ctrl Pts',(15.0885509959047,-4.84788311025075,331.604298227144));
#17841=CARTESIAN_POINT('Ctrl Pts',(15.0959484451085,-4.75566768977953,331.47630819793));
#17842=CARTESIAN_POINT('Ctrl Pts',(15.1033458943124,-4.65848285024896,331.352196812267));
#17843=CARTESIAN_POINT('Ctrl Pts',(15.1107430227758,-4.5613022244836,331.228090807857));
#17844=CARTESIAN_POINT('Ctrl Pts',(15.1181401512391,-4.45915283816774,331.107863406461));
#17845=CARTESIAN_POINT('Ctrl Pts',(15.1255372797025,-4.35238638631023,330.99192523688));
#17846=CARTESIAN_POINT('Ctrl Pts',(15.132935547139,-4.24560349508438,330.875969215715));
#17847=CARTESIAN_POINT('Ctrl Pts',(15.1403338145755,-4.13420237562885,330.76430401593));
#17848=CARTESIAN_POINT('Ctrl Pts',(15.147732082012,-4.01857252304005,330.65730435794));
#17849=CARTESIAN_POINT('Ctrl Pts',(15.1551329485376,-3.90290204846804,330.550267109845));
#17850=CARTESIAN_POINT('Ctrl Pts',(15.1625338150633,-3.7830001566908,330.447898920217));
#17851=CARTESIAN_POINT('Ctrl Pts',(15.169934681589,-3.65929030951345,330.350534977742));
#17852=CARTESIAN_POINT('Ctrl Pts',(15.1773436749736,-3.53544461709659,330.253064120349));
#17853=CARTESIAN_POINT('Ctrl Pts',(15.1847526683583,-3.40778291205219,330.160608715156));
#17854=CARTESIAN_POINT('Ctrl Pts',(15.1921616617429,-3.27675918914466,330.073461684016));
#17855=CARTESIAN_POINT('Ctrl Pts',(15.1995752193231,-3.14565475110432,329.9862609673));
#17856=CARTESIAN_POINT('Ctrl Pts',(15.2069887769032,-3.0111844862383,329.904375334482));
#17857=CARTESIAN_POINT('Ctrl Pts',(15.2144023344834,-2.873827535569,329.828052024787));
#17858=CARTESIAN_POINT('Ctrl Pts',(15.22182644662,-2.73627503213386,329.751620054889));
#17859=CARTESIAN_POINT('Ctrl Pts',(15.2292505587565,-2.5958279672626,329.680766391558));
#17860=CARTESIAN_POINT('Ctrl Pts',(15.2366746708931,-2.45298676106926,329.615690711659));
#17861=CARTESIAN_POINT('Ctrl Pts',(15.240531796049,-2.37877500354578,329.58188127595));
#17862=CARTESIAN_POINT('Ctrl Pts',(15.244388921205,-2.3039172977635,329.549630634522));
#17863=CARTESIAN_POINT('Ctrl Pts',(15.2482460463609,-2.22848537934505,329.518961460038));
#17864=CARTESIAN_POINT('Ctrl Pts',(15.2556700237989,-2.08329826775007,329.459931158919));
#17865=CARTESIAN_POINT('Ctrl Pts',(15.2630940012369,-1.93554503594606,329.406584578907));
#17866=CARTESIAN_POINT('Ctrl Pts',(15.2705179786749,-1.78571098953377,329.359151941032));
#17867=CARTESIAN_POINT('Ctrl Pts',(15.2779331947026,-1.63605376983999,329.311775280807));
#17868=CARTESIAN_POINT('Ctrl Pts',(15.2853484107303,-1.48432097594482,329.270298781773));
#17869=CARTESIAN_POINT('Ctrl Pts',(15.2927636267579,-1.33101887579755,329.234905090567));
#17870=CARTESIAN_POINT('Ctrl Pts',(15.300171707902,-1.17786428215928,329.199545454993));
#17871=CARTESIAN_POINT('Ctrl Pts',(15.3075797890461,-1.0231437495697,329.170257058716));
#17872=CARTESIAN_POINT('Ctrl Pts',(15.3149878701903,-0.867379631619293,
329.14717306448));
#17873=CARTESIAN_POINT('Ctrl Pts',(15.3223904373643,-0.711731451746692,
329.124106252082));
#17874=CARTESIAN_POINT('Ctrl Pts',(15.3297930045383,-0.555041600752708,
329.107234700991));
#17875=CARTESIAN_POINT('Ctrl Pts',(15.3371955717123,-0.397843470320487,
329.096640690622));
#17876=CARTESIAN_POINT('Ctrl Pts',(15.3445942414671,-0.240728104016909,
329.086052257952));
#17877=CARTESIAN_POINT('Ctrl Pts',(15.3519929112219,-0.0831053626589326,
329.081734808737));
#17878=CARTESIAN_POINT('Ctrl Pts',(15.3593915809767,0.07448548873379,329.083718864484));
#17879=CARTESIAN_POINT('Ctrl Pts',(15.3667890301807,0.232050342529715,329.085702592923));
#17880=CARTESIAN_POINT('Ctrl Pts',(15.3741864793847,0.38958294398263,329.093985758454));
#17881=CARTESIAN_POINT('Ctrl Pts',(15.3815839285887,0.546543149124817,329.108546771072));
#17882=CARTESIAN_POINT('Ctrl Pts',(15.3889810570522,0.703496548746151,329.12310715235));
#17883=CARTESIAN_POINT('Ctrl Pts',(15.3963781855157,0.859877229787675,329.143944805024));
#17884=CARTESIAN_POINT('Ctrl Pts',(15.4037753139792,1.0151495633807,329.170986196065));
#17885=CARTESIAN_POINT('Ctrl Pts',(15.4111735814158,1.17044580503697,329.198031750804));
#17886=CARTESIAN_POINT('Ctrl Pts',(15.4185718488525,1.32463299174301,329.231282881844));
#17887=CARTESIAN_POINT('Ctrl Pts',(15.4259701162891,1.47718523496209,329.270614837165));
#17888=CARTESIAN_POINT('Ctrl Pts',(15.4333709828149,1.62979107138849,329.309960610216));
#17889=CARTESIAN_POINT('Ctrl Pts',(15.4407718493406,1.7807604595874,329.355391367716));
#17890=CARTESIAN_POINT('Ctrl Pts',(15.4481727158663,1.92958237276239,329.406732401429));
#17891=CARTESIAN_POINT('Ctrl Pts',(15.4555817092511,2.07856770662599,329.458129812505));
#17892=CARTESIAN_POINT('Ctrl Pts',(15.4629907026359,2.22540050313096,329.515450338983));
#17893=CARTESIAN_POINT('Ctrl Pts',(15.4703996960207,2.36958875542278,329.578470723802));
#17894=CARTESIAN_POINT('Ctrl Pts',(15.477813253601,2.5138658326516,329.641529931352));
#17895=CARTESIAN_POINT('Ctrl Pts',(15.4852268111813,2.65549478446371,329.710295831364));
#17896=CARTESIAN_POINT('Ctrl Pts',(15.4926403687615,2.79400841142042,329.784499299261));
#17897=CARTESIAN_POINT('Ctrl Pts',(15.5000644808982,2.93271923788341,329.858808409379));
#17898=CARTESIAN_POINT('Ctrl Pts',(15.507488593035,3.06830556062849,329.938570359729));
#17899=CARTESIAN_POINT('Ctrl Pts',(15.5149127051717,3.20032866108321,330.023472392968));
#17900=CARTESIAN_POINT('Ctrl Pts',(15.518769830326,3.26891997710075,330.067582417444));
#17901=CARTESIAN_POINT('Ctrl Pts',(15.5226269554804,3.33655002942041,330.11307918662));
#17902=CARTESIAN_POINT('Ctrl Pts',(15.5264840806347,3.40316093185349,330.159914645959));
#17903=CARTESIAN_POINT('Ctrl Pts',(15.5339080580727,3.53136984833921,330.250060902436));
#17904=CARTESIAN_POINT('Ctrl Pts',(15.5413320355107,3.65618787737881,330.345440851766));
#17905=CARTESIAN_POINT('Ctrl Pts',(15.5487560129487,3.77715879448751,330.445770975925));
#17906=CARTESIAN_POINT('Ctrl Pts',(15.5561712289763,3.89798694771296,330.545982695442));
#17907=CARTESIAN_POINT('Ctrl Pts',(15.563586445004,4.01497674181611,330.651132725357));
#17908=CARTESIAN_POINT('Ctrl Pts',(15.5710016610316,4.12770061470438,330.760894174726));
#17909=CARTESIAN_POINT('Ctrl Pts',(15.5784097421757,4.24031602524981,330.870550012182));
#17910=CARTESIAN_POINT('Ctrl Pts',(15.5858178233199,4.34867342056585,330.984808177061));
#17911=CARTESIAN_POINT('Ctrl Pts',(15.593225904464,4.45237814576104,331.103301473087));
#17912=CARTESIAN_POINT('Ctrl Pts',(15.600628471638,4.55600568163524,331.221706572388));
#17913=CARTESIAN_POINT('Ctrl Pts',(15.608031038812,4.65498719812048,331.344340246535));
#17914=CARTESIAN_POINT('Ctrl Pts',(15.6154336059861,4.74896485585733,331.470798481196));
#17915=CARTESIAN_POINT('Ctrl Pts',(15.6228322757408,4.84289303476812,331.597190136148));
#17916=CARTESIAN_POINT('Ctrl Pts',(15.6302309454956,4.93182237966197,331.727402042584));
#17917=CARTESIAN_POINT('Ctrl Pts',(15.6376296152504,5.01543539710643,331.860997237983));
#17918=CARTESIAN_POINT('Ctrl Pts',(15.6450270644544,5.09903462099934,331.994570394323));
#17919=CARTESIAN_POINT('Ctrl Pts',(15.6524245136583,5.17731906025537,332.131525415852));
#17920=CARTESIAN_POINT('Ctrl Pts',(15.6598219628623,5.25001456747629,332.271396400393));
#17921=CARTESIAN_POINT('Ctrl Pts',(15.6672190913258,5.32270692274676,332.411261320373));
#17922=CARTESIAN_POINT('Ctrl Pts',(15.6746162197893,5.3898106556944,332.554041620822));
#17923=CARTESIAN_POINT('Ctrl Pts',(15.6820133482528,5.45109774229761,332.699247087057));
#17924=CARTESIAN_POINT('Ctrl Pts',(15.6894116156894,5.51239426558222,332.844474911308));
#17925=CARTESIAN_POINT('Ctrl Pts',(15.696809883126,5.56787221409481,332.992128301003));
#17926=CARTESIAN_POINT('Ctrl Pts',(15.7042081505626,5.6173519060064,333.141697514777));
#17927=CARTESIAN_POINT('Ctrl Pts',(15.7116090170884,5.66684898065418,333.291319273788));
#17928=CARTESIAN_POINT('Ctrl Pts',(15.7190098836142,5.7103434860261,333.442857842815));
#17929=CARTESIAN_POINT('Ctrl Pts',(15.72641075014,5.74770579208278,333.59578894387));
#17930=CARTESIAN_POINT('Ctrl Pts',(15.7338197435248,5.78510912552349,333.748887977895));
#17931=CARTESIAN_POINT('Ctrl Pts',(15.7412287369095,5.81636672338197,333.903382234944));
#17932=CARTESIAN_POINT('Ctrl Pts',(15.7486377302943,5.84140007414198,334.058737158752));
#17933=CARTESIAN_POINT('Ctrl Pts',(15.7560512878746,5.86644884630955,334.214187786552));
#17934=CARTESIAN_POINT('Ctrl Pts',(15.7634648454549,5.88526568642664,334.370499767935));
#17935=CARTESIAN_POINT('Ctrl Pts',(15.7708784030351,5.8978240786673,334.527134586175));
#17936=CARTESIAN_POINT('Ctrl Pts',(15.7783025151718,5.91040035007842,334.683992402754));
#17937=CARTESIAN_POINT('Ctrl Pts',(15.7857266273085,5.9167003635619,334.841173602231));
#17938=CARTESIAN_POINT('Ctrl Pts',(15.7931507394453,5.91674970764539,334.998140005856));
#17939=CARTESIAN_POINT('Ctrl Pts',(15.7970078645998,5.91677534388339,335.079690372107));
#17940=CARTESIAN_POINT('Ctrl Pts',(15.8008649897542,5.91511464197454,335.161182838334));
#17941=CARTESIAN_POINT('Ctrl Pts',(15.8047221149087,5.91177668646496,335.242542721741));
#17942=CARTESIAN_POINT('Ctrl Pts',(15.8121460923467,5.90535197754329,335.399139646802));
#17943=CARTESIAN_POINT('Ctrl Pts',(15.8195700697847,5.89269114088026,335.555717353779));
#17944=CARTESIAN_POINT('Ctrl Pts',(15.8269940472227,5.87378570358288,335.7117387659));
#17945=CARTESIAN_POINT('Ctrl Pts',(15.8344092632503,5.854902577546,335.867576049281));
#17946=CARTESIAN_POINT('Ctrl Pts',(15.8418244792779,5.8297895645756,336.022857977704));
#17947=CARTESIAN_POINT('Ctrl Pts',(15.8492396953056,5.79849017585737,336.177048105638));
#17948=CARTESIAN_POINT('Ctrl Pts',(15.8566477764496,5.7672209032534,336.331089872607));
#17949=CARTESIAN_POINT('Ctrl Pts',(15.8640558575937,5.72977717896721,336.48404156718));
#17950=CARTESIAN_POINT('Ctrl Pts',(15.8714639387378,5.68625421577511,336.635372604662));
#17951=CARTESIAN_POINT('Ctrl Pts',(15.8788665059118,5.6427636475194,336.78659100369));
#17952=CARTESIAN_POINT('Ctrl Pts',(15.8862690730858,5.59320295278255,336.93619079038));
#17953=CARTESIAN_POINT('Ctrl Pts',(15.8936716402598,5.53771822842728,337.083652414642));
#17954=CARTESIAN_POINT('Ctrl Pts',(15.9010703100146,5.48226271653681,337.231036401004));
#17955=CARTESIAN_POINT('Ctrl Pts',(15.9084689797693,5.42088951775276,337.37628411848));
#17956=CARTESIAN_POINT('Ctrl Pts',(15.915867649524,5.35379426926663,337.518892114575));
#17957=CARTESIAN_POINT('Ctrl Pts',(15.923265098728,5.28671008941308,337.661476584779));
#17958=CARTESIAN_POINT('Ctrl Pts',(15.930662547932,5.21390589204398,337.801421860501));
#17959=CARTESIAN_POINT('Ctrl Pts',(15.938059997136,5.13562510735151,337.938245278945));
#17960=CARTESIAN_POINT('Ctrl Pts',(15.9454571255995,5.0573477167775,338.075062764963));
#17961=CARTESIAN_POINT('Ctrl Pts',(15.9528542540629,4.9735943963554,338.208758338899));
#17962=CARTESIAN_POINT('Ctrl Pts',(15.9602513825264,4.88465398118969,338.338874967193));
#17963=CARTESIAN_POINT('Ctrl Pts',(15.967649649963,4.79569987142016,338.4690116302));
#17964=CARTESIAN_POINT('Ctrl Pts',(15.9750479173995,4.70155728724309,338.595567942188));
#17965=CARTESIAN_POINT('Ctrl Pts',(15.9824461848361,4.60255764489959,338.718116954572));
#17966=CARTESIAN_POINT('Ctrl Pts',(15.9898470513619,4.50352322294063,338.840709019713));
#17967=CARTESIAN_POINT('Ctrl Pts',(15.9972479178877,4.39962857988415,338.959290692176));
#17968=CARTESIAN_POINT('Ctrl Pts',(16.0046487844134,4.2912444420216,339.073469246394));
#17969=CARTESIAN_POINT('Ctrl Pts',(16.0120577777982,4.18274128801374,339.187773179581));
#17970=CARTESIAN_POINT('Ctrl Pts',(16.0194667711829,4.06973905103298,339.297664067839));
#17971=CARTESIAN_POINT('Ctrl Pts',(16.0268757645676,3.95264476376096,339.402786610093));
#17972=CARTESIAN_POINT('Ctrl Pts',(16.0342893221479,3.83547834236897,339.507973911458));
#17973=CARTESIAN_POINT('Ctrl Pts',(16.0417028797281,3.71421513435229,339.608386776058));
#17974=CARTESIAN_POINT('Ctrl Pts',(16.0491164373084,3.58929364067983,339.703711483868));
#17975=CARTESIAN_POINT('Ctrl Pts',(16.0565405494451,3.46419429839136,339.799171903851));
#17976=CARTESIAN_POINT('Ctrl Pts',(16.0639646615817,3.33542657322832,339.889529485687));
#17977=CARTESIAN_POINT('Ctrl Pts',(16.0713887737184,3.20345687860428,339.974514507912));
#17978=CARTESIAN_POINT('Ctrl Pts',(16.0752458988732,3.1348933090586,340.018667648511));
#17979=CARTESIAN_POINT('Ctrl Pts',(16.0791030240279,3.06546585454412,340.061371378362));
#17980=CARTESIAN_POINT('Ctrl Pts',(16.0829601491827,2.99524223358791,340.102592921705));
#17981=CARTESIAN_POINT('Ctrl Pts',(16.0903841266206,2.86007975980807,340.181933828587));
#17982=CARTESIAN_POINT('Ctrl Pts',(16.0978081040587,2.72155872037476,340.256020242603));
#17983=CARTESIAN_POINT('Ctrl Pts',(16.1052320814967,2.58012616943561,340.324554395655));
#17984=CARTESIAN_POINT('Ctrl Pts',(16.1126472975243,2.43886053018624,340.393007668096));
#17985=CARTESIAN_POINT('Ctrl Pts',(16.1200625135519,2.29469055147802,340.455921561271));
#17986=CARTESIAN_POINT('Ctrl Pts',(16.1274777295795,2.14809088820202,340.513042363208));
#17987=CARTESIAN_POINT('Ctrl Pts',(16.1348858107236,2.001632282384,340.570108203796));
#17988=CARTESIAN_POINT('Ctrl Pts',(16.1422938918677,1.85274899160489,340.621391915517));
#17989=CARTESIAN_POINT('Ctrl Pts',(16.1497019730118,1.70193872094931,340.666686435002));
#17990=CARTESIAN_POINT('Ctrl Pts',(16.1571045401858,1.55124070113231,340.711947240949));
#17991=CARTESIAN_POINT('Ctrl Pts',(16.1645071073598,1.39861891321875,340.751227624025));
#17992=CARTESIAN_POINT('Ctrl Pts',(16.1719096745338,1.24458931935898,340.784369281835));
#17993=CARTESIAN_POINT('Ctrl Pts',(16.1793083442885,1.0906408214072,340.817493490707));
#17994=CARTESIAN_POINT('Ctrl Pts',(16.1867070140433,0.935286357602493,340.844485332748));
#17995=CARTESIAN_POINT('Ctrl Pts',(16.194105683798,0.779055162397271,340.865236876414));
#17996=CARTESIAN_POINT('Ctrl Pts',(16.201503133002,0.62284974048802,340.885984996719));
#17997=CARTESIAN_POINT('Ctrl Pts',(16.208900582206,0.465768243831204,340.900494812694));
#17998=CARTESIAN_POINT('Ctrl Pts',(16.2162980314099,0.308348287915098,340.908709833444));
#17999=CARTESIAN_POINT('Ctrl Pts',(16.2236951598734,0.150935157453836,340.916924498006));
#18000=CARTESIAN_POINT('Ctrl Pts',(16.2310922883369,-0.00681603038382703,
340.918844890571));
#18001=CARTESIAN_POINT('Ctrl Pts',(16.2384894168004,-0.164364641079509,
340.914466571658));
#18002=CARTESIAN_POINT('Ctrl Pts',(16.245887684237,-0.321937510328295,340.910087578594));
#18003=CARTESIAN_POINT('Ctrl Pts',(16.2532859516736,-0.479307367238124,
340.899407953332));
#18004=CARTESIAN_POINT('Ctrl Pts',(16.2606842191102,-0.635935833290562,
340.882475344482));
#18005=CARTESIAN_POINT('Ctrl Pts',(16.2680850856359,-0.792619324570043,
340.865536787029));
#18006=CARTESIAN_POINT('Ctrl Pts',(16.2754859521616,-0.948560535604319,
340.842340912372));
#18007=CARTESIAN_POINT('Ctrl Pts',(16.2828868186874,-1.10322859381684,340.812986945821));
#18008=CARTESIAN_POINT('Ctrl Pts',(16.2902958120721,-1.25806649234457,340.783600745808));
#18009=CARTESIAN_POINT('Ctrl Pts',(16.2977048054569,-1.41162807919804,340.748043019108));
#18010=CARTESIAN_POINT('Ctrl Pts',(16.3051137988417,-1.56339430538188,340.706463774388));
#18011=CARTESIAN_POINT('Ctrl Pts',(16.3125273564219,-1.71525402479601,340.664858915418));
#18012=CARTESIAN_POINT('Ctrl Pts',(16.3199409140022,-1.86531582479206,340.617225259484));
#18013=CARTESIAN_POINT('Ctrl Pts',(16.3273544715824,-2.01307859347319,340.563761779498));
#18014=CARTESIAN_POINT('Ctrl Pts',(16.3347785837191,-2.16105172950692,340.51022218446));
#18015=CARTESIAN_POINT('Ctrl Pts',(16.3422026958558,-2.30671895254345,340.45083632948));
#18016=CARTESIAN_POINT('Ctrl Pts',(16.3496268079925,-2.44960104498864,340.385850469786));
#18017=CARTESIAN_POINT('Ctrl Pts',(16.3534839331471,-2.52383404454175,340.352087699301));
#18018=CARTESIAN_POINT('Ctrl Pts',(16.3573410583018,-2.59731570140048,340.316814110192));
#18019=CARTESIAN_POINT('Ctrl Pts',(16.3611981834565,-2.66998180734956,340.280068911569));
#18020=CARTESIAN_POINT('Ctrl Pts',(16.3686221608945,-2.80984543879467,340.209343821098));
#18021=CARTESIAN_POINT('Ctrl Pts',(16.3760461383325,-2.94710796767754,340.132950933523));
#18022=CARTESIAN_POINT('Ctrl Pts',(16.3834701157705,-3.08127706780265,340.051105046812));
#18023=CARTESIAN_POINT('Ctrl Pts',(16.3908853317981,-3.21528782820279,339.969355750563));
#18024=CARTESIAN_POINT('Ctrl Pts',(16.3983005478257,-3.3462121111337,339.882166457331));
#18025=CARTESIAN_POINT('Ctrl Pts',(16.4057157638534,-3.47357970178658,339.789799016434));
#18026=CARTESIAN_POINT('Ctrl Pts',(16.4131238449974,-3.60082473998494,339.697520451024));
#18027=CARTESIAN_POINT('Ctrl Pts',(16.4205319261416,-3.72451959882275,339.600073874593));
#18028=CARTESIAN_POINT('Ctrl Pts',(16.4279400072857,-3.84422081751713,339.497765764095));
#18029=CARTESIAN_POINT('Ctrl Pts',(16.4353425744597,-3.96383294040825,339.395533803393));
#18030=CARTESIAN_POINT('Ctrl Pts',(16.4427451416336,-4.0794570594239,339.288447755084));
#18031=CARTESIAN_POINT('Ctrl Pts',(16.4501477088076,-4.19068083797589,339.176855836239));
#18032=CARTESIAN_POINT('Ctrl Pts',(16.4575463785624,-4.30184605769473,339.065322670051));
#18033=CARTESIAN_POINT('Ctrl Pts',(16.4649450483171,-4.40861528811464,338.949288621615));
#18034=CARTESIAN_POINT('Ctrl Pts',(16.4723437180718,-4.51061136816778,338.829140327522));
#18035=CARTESIAN_POINT('Ctrl Pts',(16.4797411672758,-4.61259062203485,338.709011854166));
#18036=CARTESIAN_POINT('Ctrl Pts',(16.4871386164798,-4.7097980470165,338.584770766438));
#18037=CARTESIAN_POINT('Ctrl Pts',(16.4945360656838,-4.80189520412677,338.456838586206));
#18038=CARTESIAN_POINT('Ctrl Pts',(16.5019331941473,-4.89398836806486,338.328911952891));
#18039=CARTESIAN_POINT('Ctrl Pts',(16.5093303226107,-4.98097148664305,338.197294848174));
#18040=CARTESIAN_POINT('Ctrl Pts',(16.5167274510742,-5.0625482582468,338.062439500696));
#18041=CARTESIAN_POINT('Ctrl Pts',(16.5241257185108,-5.14413759063696,337.927563388861));
#18042=CARTESIAN_POINT('Ctrl Pts',(16.5315239859474,-5.22031872536865,337.789448360821));
#18043=CARTESIAN_POINT('Ctrl Pts',(16.538922253384,-5.29084038366606,337.648572935954));
#18044=CARTESIAN_POINT('Ctrl Pts',(16.5463231199098,-5.36138681696366,337.507648020069));
#18045=CARTESIAN_POINT('Ctrl Pts',(16.5537239864355,-5.4262696482983,337.363961110095));
#18046=CARTESIAN_POINT('Ctrl Pts',(16.5611248529613,-5.48528503273618,337.218012324614));
#18047=CARTESIAN_POINT('Ctrl Pts',(16.568533846346,-5.54436522170827,337.071903273414));
#18048=CARTESIAN_POINT('Ctrl Pts',(16.5759428397308,-5.59756495674408,336.923527732717));
#18049=CARTESIAN_POINT('Ctrl Pts',(16.5833518331155,-5.64472949613641,336.773403360194));
#18050=CARTESIAN_POINT('Ctrl Pts',(16.5907653906957,-5.69192309051188,336.623186505879));
#18051=CARTESIAN_POINT('Ctrl Pts',(16.598178948276,-5.73307398353923,336.47121903239));
#18052=CARTESIAN_POINT('Ctrl Pts',(16.6055925058562,-5.76807831538502,336.318030011071));
#18053=CARTESIAN_POINT('Ctrl Pts',(16.6130166179929,-5.80313248230559,336.164622897136));
#18054=CARTESIAN_POINT('Ctrl Pts',(16.6204407301296,-5.83202254267949,336.009991127921));
#18055=CARTESIAN_POINT('Ctrl Pts',(16.6278648422663,-5.85469624564492,335.85467095056));
#18056=CARTESIAN_POINT('Ctrl Pts',(16.631721967421,-5.86647614719388,335.773975865127));
#18057=CARTESIAN_POINT('Ctrl Pts',(16.6355790925757,-5.87657897448611,335.693095009146));
#18058=CARTESIAN_POINT('Ctrl Pts',(16.6394362177305,-5.88500295254959,335.612103594976));
#18059=CARTESIAN_POINT('Ctrl Pts',(16.6490580185851,-5.906017007339,335.410066267478));
#18060=CARTESIAN_POINT('Ctrl Pts',(16.6586798194398,-5.91662935509008,335.206928493545));
#18061=CARTESIAN_POINT('Ctrl Pts',(16.6683016202945,-5.91674897726595,335.003478867974));
#18062=CARTESIAN_POINT('',(18.4183016202946,-5.90876483699497,335.00325795821));
#18063=CARTESIAN_POINT('Ctrl Pts',(16.6683041419001,-5.92392104138316,335.003429701801));
#18064=CARTESIAN_POINT('Ctrl Pts',(16.7514275119349,-5.91162770464222,333.243676356358));
#18065=CARTESIAN_POINT('Ctrl Pts',(16.9272968933942,-4.14640825180893,329.499088905554));
#18066=CARTESIAN_POINT('Ctrl Pts',(17.1959122862784,2.22434875857224,328.366381415739));
#18067=CARTESIAN_POINT('Ctrl Pts',(17.4741503205522,6.78207413591985,333.280670672585));
#18068=CARTESIAN_POINT('Ctrl Pts',(17.7523883548264,5.11599018198272,339.772763075944));
#18069=CARTESIAN_POINT('Ctrl Pts',(18.0306263891,-1.24496245006616,341.884961250371));
#18070=CARTESIAN_POINT('Ctrl Pts',(18.2525974775897,-5.40812166706467,338.52950027048));
#18071=CARTESIAN_POINT('Ctrl Pts',(18.3818225546544,-5.91264194830766,335.780609200208));
#18072=CARTESIAN_POINT('Ctrl Pts',(18.4183016202946,-5.90876483699497,335.00325795821));
#18073=CARTESIAN_POINT('',(20.1683016202945,-5.91198872894514,334.99513445012));
#18074=CARTESIAN_POINT('Ctrl Pts',(18.4183016202946,-5.90876483699497,335.00325795821));
#18075=CARTESIAN_POINT('Ctrl Pts',(18.474568566079,-5.90278460673951,333.804236562747));
#18076=CARTESIAN_POINT('Ctrl Pts',(18.6235815232882,-4.96516095045598,330.620246725548));
#18077=CARTESIAN_POINT('Ctrl Pts',(18.8653404919221,0.239575224204735,328.007487816731));
#18078=CARTESIAN_POINT('Ctrl Pts',(19.143578526196,6.00980057425877,331.417414344516));
#18079=CARTESIAN_POINT('Ctrl Pts',(19.4218165604697,6.26492064182342,338.115026849459));
#18080=CARTESIAN_POINT('Ctrl Pts',(19.7000545947439,0.77081550646824,341.954025192377));
#18081=CARTESIAN_POINT('Ctrl Pts',(19.9488829480187,-4.77516190733568,339.680170192244));
#18082=CARTESIAN_POINT('Ctrl Pts',(20.1049652898689,-5.90157873863965,336.342952334915));
#18083=CARTESIAN_POINT('Ctrl Pts',(20.1683016202945,-5.91198872894514,334.99513445012));
#18084=CARTESIAN_POINT('',(21.9183016202945,-5.92629064703929,334.99899238386));
#18085=CARTESIAN_POINT('Ctrl Pts',(20.1683016202945,-5.91198872894514,334.99513445012));
#18086=CARTESIAN_POINT('Ctrl Pts',(20.1977113012936,-5.91682251852579,334.369286792539));
#18087=CARTESIAN_POINT('Ctrl Pts',(20.3198669937171,-5.53687134207544,331.775491648162));
#18088=CARTESIAN_POINT('Ctrl Pts',(20.5347686975658,-1.76510783169628,328.229695925316));
#18089=CARTESIAN_POINT('Ctrl Pts',(20.8130067318395,4.7380920049118,329.851883152624));
#18090=CARTESIAN_POINT('Ctrl Pts',(21.0912447661135,6.89321474273118,336.19842122469));
#18091=CARTESIAN_POINT('Ctrl Pts',(21.3694828003874,2.72253605483465,341.445185827526));
#18092=CARTESIAN_POINT('Ctrl Pts',(21.6451684184478,-3.88539471633639,340.783425390433));
#18093=CARTESIAN_POINT('Ctrl Pts',(21.8281080250835,-5.92180424765322,336.906401464071));
#18094=CARTESIAN_POINT('Ctrl Pts',(21.9183016202945,-5.92629064703929,334.99899238386));
#18095=CARTESIAN_POINT('',(23.6683016202945,-5.91500612781905,335.00540571853));
#18096=CARTESIAN_POINT('Ctrl Pts',(21.9183016202945,-5.92629064703929,334.99899238386));
#18097=CARTESIAN_POINT('Ctrl Pts',(21.9208540365081,-5.92641760903151,334.945014029289));
#18098=CARTESIAN_POINT('Ctrl Pts',(21.9234064527217,-5.92574411097084,334.891038923218));
#18099=CARTESIAN_POINT('Ctrl Pts',(22.01870488036,-5.87034887063351,332.876626256431));
#18100=CARTESIAN_POINT('Ctrl Pts',(22.2041969032092,-3.62310438234698,329.014539486737));
#18101=CARTESIAN_POINT('Ctrl Pts',(22.4824349374833,3.07263176483227,328.714178099963));
#18102=CARTESIAN_POINT('Ctrl Pts',(22.7606729717571,6.94865909339069,334.182222692275));
#18103=CARTESIAN_POINT('Ctrl Pts',(23.038911006031,4.44800453399053,340.400729449511));
#18104=CARTESIAN_POINT('Ctrl Pts',(23.3171490403051,-2.13451813381742,341.663066505569));
#18105=CARTESIAN_POINT('Ctrl Pts',(23.5269459117261,-5.62088275218896,338.004367855669));
#18106=CARTESIAN_POINT('Ctrl Pts',(23.6439967717226,-5.91961735110844,335.521952838584));
#18107=CARTESIAN_POINT('Ctrl Pts',(23.6683016202945,-5.91500612781905,335.00540571853));
#18108=CARTESIAN_POINT('',(25.4183016202945,-5.90739708893958,334.998339410743));
#18109=CARTESIAN_POINT('Ctrl Pts',(23.6683016202945,-5.91500612781905,335.00540571853));
#18110=CARTESIAN_POINT('Ctrl Pts',(23.7367427831473,-5.90202116791829,333.550836460046));
#18111=CARTESIAN_POINT('Ctrl Pts',(23.8979299574247,-4.62690565408727,330.104798499186));
#18112=CARTESIAN_POINT('Ctrl Pts',(24.151863143127,1.15182530317369,328.098846372365));
#18113=CARTESIAN_POINT('Ctrl Pts',(24.4301011774006,6.42664607839832,332.233984254528));
#18114=CARTESIAN_POINT('Ctrl Pts',(24.7083392116747,5.80382860462329,338.907453959981));
#18115=CARTESIAN_POINT('Ctrl Pts',(24.9865772459487,-0.14507671524839,341.995110840288));
#18116=CARTESIAN_POINT('Ctrl Pts',(25.2232313821552,-5.09165478374774,339.161387958908));
#18117=CARTESIAN_POINT('Ctrl Pts',(25.3671395069372,-5.90466232056242,336.089210272338));
#18118=CARTESIAN_POINT('Ctrl Pts',(25.4183016202945,-5.90739708893958,334.998339410743));
#18119=CARTESIAN_POINT('',(27.1683016202945,-5.92111329140699,334.99527144238));
#18120=CARTESIAN_POINT('Ctrl Pts',(25.4183016202945,-5.90739708893958,334.998339410743));
#18121=CARTESIAN_POINT('Ctrl Pts',(25.4598855183618,-5.90961987298759,334.111693810387));
#18122=CARTESIAN_POINT('Ctrl Pts',(25.594215427854,-5.30581593151386,331.250407457081));
#18123=CARTESIAN_POINT('Ctrl Pts',(25.8212913487704,-0.864701785489386,
328.057024143541));
#18124=CARTESIAN_POINT('Ctrl Pts',(26.0995293830443,5.3705567668813,330.515611197175));
#18125=CARTESIAN_POINT('Ctrl Pts',(26.3777674173184,6.67733464357878,337.089455665694));
#18126=CARTESIAN_POINT('Ctrl Pts',(26.6560054515924,1.85642107515762,341.745837510118));
#18127=CARTESIAN_POINT('Ctrl Pts',(26.9195168525843,-4.32277153150168,340.292864862948));
#18128=CARTESIAN_POINT('Ctrl Pts',(27.0902822421518,-5.90669512999897,336.649017329653));
#18129=CARTESIAN_POINT('Ctrl Pts',(27.1683016202945,-5.92111329140699,334.99527144238));
#18130=CARTESIAN_POINT('',(28.9183016202945,-5.92262096125729,335.004164858762));
#18131=CARTESIAN_POINT('Ctrl Pts',(27.1683016202945,-5.92111329140699,334.99527144238));
#18132=CARTESIAN_POINT('Ctrl Pts',(27.1830282535764,-5.92383480727534,334.683116823835));
#18133=CARTESIAN_POINT('Ctrl Pts',(27.290500898283,-5.75928232400781,332.407936679943));
#18134=CARTESIAN_POINT('Ctrl Pts',(27.490719554414,-2.809369194695,328.592186983913));
#18135=CARTESIAN_POINT('Ctrl Pts',(27.7689575886882,3.86815579710411,329.169906205681));
#18136=CARTESIAN_POINT('Ctrl Pts',(28.0471956229618,6.99593130778298,335.097816450449));
#18137=CARTESIAN_POINT('Ctrl Pts',(28.3254336572358,3.70364391709208,340.935961982409));
#18138=CARTESIAN_POINT('Ctrl Pts',(28.6036716915099,-2.98742283062345,341.326762817769));
#18139=CARTESIAN_POINT('Ctrl Pts',(28.8012943458627,-5.79265084944902,337.480554438737));
#18140=CARTESIAN_POINT('Ctrl Pts',(28.9061709887909,-5.9246739829894,335.261122693151));
#18141=CARTESIAN_POINT('Ctrl Pts',(28.9183016202945,-5.92262096125729,335.004164858762));
#18142=CARTESIAN_POINT('',(30.6683016202945,-5.90798040082929,335.002506028461));
#18143=CARTESIAN_POINT('Ctrl Pts',(28.9183016202945,-5.92262096125729,335.004164858762));
#18144=CARTESIAN_POINT('Ctrl Pts',(28.9989170002156,-5.90897739069207,333.296524705252));
#18145=CARTESIAN_POINT('Ctrl Pts',(29.1722783915612,-4.23435313665628,329.600953149295));
#18146=CARTESIAN_POINT('Ctrl Pts',(29.4383857943318,2.04429783446821,328.308701973068));
#18147=CARTESIAN_POINT('Ctrl Pts',(29.7166238286054,6.73314212344229,333.098048353212));
#18148=CARTESIAN_POINT('Ctrl Pts',(29.9948618628796,5.24308126675361,339.632787686851));
#18149=CARTESIAN_POINT('Ctrl Pts',(30.2730998971534,-1.05847788068605,341.916086140104));
#18150=CARTESIAN_POINT('Ctrl Pts',(30.4975798162917,-5.35884259352751,338.637697927416));
#18151=CARTESIAN_POINT('Ctrl Pts',(30.6293137240055,-5.91114314230631,335.833595143404));
#18152=CARTESIAN_POINT('Ctrl Pts',(30.6683016202945,-5.90798040082929,335.002506028461));
#18153=CARTESIAN_POINT('',(32.418301636369,-5.91460742755292,334.994794146473));
#18154=CARTESIAN_POINT('Ctrl Pts',(30.6683016202945,-5.90798040082929,335.002506028461));
#18155=CARTESIAN_POINT('Ctrl Pts',(30.7220597354301,-5.90361948278424,333.856566170669));
#18156=CARTESIAN_POINT('Ctrl Pts',(30.8685638619903,-5.02842874153069,330.727440116774));
#18157=CARTESIAN_POINT('Ctrl Pts',(31.1078139999753,0.0505517212931561,
328.003567520179));
#18158=CARTESIAN_POINT('Ctrl Pts',(31.386052034249,5.91080577166923,331.256338950865));
#18159=CARTESIAN_POINT('Ctrl Pts',(31.6642900685232,6.34680060873793,337.944612869997));
#18160=CARTESIAN_POINT('Ctrl Pts',(31.942528102797,0.958430205788535,341.930659020746));
#18161=CARTESIAN_POINT('Ctrl Pts',(32.1938652867209,-4.70347817982554,339.786078150809));
#18162=CARTESIAN_POINT('Ctrl Pts',(32.35245645922,-5.90164065851028,336.395145633034));
#18163=CARTESIAN_POINT('Ctrl Pts',(32.4183016202945,-5.91341914242724,334.994795534346));
#18164=CARTESIAN_POINT('',(34.1683016202624,-5.91674999997471,334.999982700985));
#18165=CARTESIAN_POINT('Ctrl Pts',(32.4183016653215,-5.91674770761404,334.994791646704));
#18166=CARTESIAN_POINT('Ctrl Pts',(32.4273153323639,-5.91657886872254,334.802988774011));
#18167=CARTESIAN_POINT('Ctrl Pts',(32.4363289994064,-5.9070798724418,334.611596525586));
#18168=CARTESIAN_POINT('Ctrl Pts',(32.4453426664488,-5.88839253570148,334.421412143236));
#18169=CARTESIAN_POINT('Ctrl Pts',(32.4544843738112,-5.86943974289714,334.228526166845));
#18170=CARTESIAN_POINT('Ctrl Pts',(32.4636260811736,-5.84103576178567,334.036882586459));
#18171=CARTESIAN_POINT('Ctrl Pts',(32.472767788536,-5.80337755149894,333.847290341301));
#18172=CARTESIAN_POINT('Ctrl Pts',(32.4815132494723,-5.76735163271395,333.665915953769));
#18173=CARTESIAN_POINT('Ctrl Pts',(32.4902587104086,-5.7228567391478,333.486418710041));
#18174=CARTESIAN_POINT('Ctrl Pts',(32.499004171345,-5.67010589101885,333.309488317954));
#18175=CARTESIAN_POINT('Ctrl Pts',(32.506428148783,-5.6253259635575,333.159293005378));
#18176=CARTESIAN_POINT('Ctrl Pts',(32.513852126221,-5.57450658153742,333.010651606305));
#18177=CARTESIAN_POINT('Ctrl Pts',(32.5212761036589,-5.51777175704479,332.864086752778));
#18178=CARTESIAN_POINT('Ctrl Pts',(32.5286913196866,-5.46110388818127,332.71769486783));
#18179=CARTESIAN_POINT('Ctrl Pts',(32.5361065357142,-5.39853460627703,332.573374995057));
#18180=CARTESIAN_POINT('Ctrl Pts',(32.5435217517418,-5.33023815207165,332.431636356608));
#18181=CARTESIAN_POINT('Ctrl Pts',(32.5509298328859,-5.26200741237057,332.290034098363));
#18182=CARTESIAN_POINT('Ctrl Pts',(32.55833791403,-5.18806063197998,332.151008463924));
#18183=CARTESIAN_POINT('Ctrl Pts',(32.5657459951741,-5.1086207190128,332.015050266458));
#18184=CARTESIAN_POINT('Ctrl Pts',(32.5731485623481,-5.0292399346237,331.879193265161));
#18185=CARTESIAN_POINT('Ctrl Pts',(32.5805511295221,-4.94437434620895,331.746399475609));
#18186=CARTESIAN_POINT('Ctrl Pts',(32.5879536966961,-4.85429346317123,331.617136488725));
#18187=CARTESIAN_POINT('Ctrl Pts',(32.5953523664508,-4.76426000732511,331.48794155824));
#18188=CARTESIAN_POINT('Ctrl Pts',(32.6027510362055,-4.66901693818283,331.362274033633));
#18189=CARTESIAN_POINT('Ctrl Pts',(32.6101497059602,-4.56887781756843,331.240573707249));
#18190=CARTESIAN_POINT('Ctrl Pts',(32.6175471551641,-4.46875521679902,331.118893457638));
#18191=CARTESIAN_POINT('Ctrl Pts',(32.6249446043681,-4.36373840447703,331.001179395262));
#18192=CARTESIAN_POINT('Ctrl Pts',(32.632342053572,-4.25418214614182,330.887839396382));
#18193=CARTESIAN_POINT('Ctrl Pts',(32.6397391820355,-4.14463063797514,330.774504311727));
#18194=CARTESIAN_POINT('Ctrl Pts',(32.6471363104989,-4.03054033452622,330.66554318182));
#18195=CARTESIAN_POINT('Ctrl Pts',(32.6545334389624,-3.91230369900613,330.561327864187));
#18196=CARTESIAN_POINT('Ctrl Pts',(32.661931706399,-3.79404885799557,330.457096499996));
#18197=CARTESIAN_POINT('Ctrl Pts',(32.6693299738356,-3.67164669370789,330.357612649864));
#18198=CARTESIAN_POINT('Ctrl Pts',(32.6767282412721,-3.54552353319519,330.263208529177));
#18199=CARTESIAN_POINT('Ctrl Pts',(32.6841291077979,-3.41935606428986,330.16877124333));
#18200=CARTESIAN_POINT('Ctrl Pts',(32.6915299743236,-3.28946529507127,330.07941746349));
#18201=CARTESIAN_POINT('Ctrl Pts',(32.6989308408493,-3.15630722727234,329.995436557544));
#18202=CARTESIAN_POINT('Ctrl Pts',(32.7063398342341,-3.02300293918437,329.911363432534));
#18203=CARTESIAN_POINT('Ctrl Pts',(32.7137488276188,-2.88642450333695,329.832675163101));
#18204=CARTESIAN_POINT('Ctrl Pts',(32.7211578210036,-2.74705389675535,329.759615906174));
#18205=CARTESIAN_POINT('Ctrl Pts',(32.7285713785838,-2.60759743307269,329.686511642226));
#18206=CARTESIAN_POINT('Ctrl Pts',(32.735984936164,-2.46534570760064,329.619043460126));
#18207=CARTESIAN_POINT('Ctrl Pts',(32.7433984937442,-2.32080096015193,329.557407468324));
#18208=CARTESIAN_POINT('Ctrl Pts',(32.7508226058809,-2.17605042679298,329.495683726404));
#18209=CARTESIAN_POINT('Ctrl Pts',(32.7582467180176,-2.02900069945885,329.439808890119));
#18210=CARTESIAN_POINT('Ctrl Pts',(32.7656708301542,-1.88017023918067,329.389929551761));
#18211=CARTESIAN_POINT('Ctrl Pts',(32.7695279553091,-1.80284682304979,329.364015227308));
#18212=CARTESIAN_POINT('Ctrl Pts',(32.7733850804639,-1.72504294531009,329.339718384046));
#18213=CARTESIAN_POINT('Ctrl Pts',(32.7772422056188,-1.64683230932039,329.317054117143));
#18214=CARTESIAN_POINT('Ctrl Pts',(32.7846661830568,-1.49629687847732,329.273431211643));
#18215=CARTESIAN_POINT('Ctrl Pts',(32.7920901604948,-1.3437998712445,329.235727924088));
#18216=CARTESIAN_POINT('Ctrl Pts',(32.7995141379328,-1.18984789011225,329.204122796255));
#18217=CARTESIAN_POINT('Ctrl Pts',(32.8069293539605,-1.03607759548106,329.172554967228));
#18218=CARTESIAN_POINT('Ctrl Pts',(32.8143445699881,-0.880856106873434,
329.147071047008));
#18219=CARTESIAN_POINT('Ctrl Pts',(32.8217597860157,-0.724705931719506,
329.127800082164));
#18220=CARTESIAN_POINT('Ctrl Pts',(32.8291678671598,-0.568706003477776,
329.108547659746));
#18221=CARTESIAN_POINT('Ctrl Pts',(32.836575948304,-0.411779535561657,329.095496336878));
#18222=CARTESIAN_POINT('Ctrl Pts',(32.8439840294481,-0.254459891602752,
329.088724272539));
#18223=CARTESIAN_POINT('Ctrl Pts',(32.8513865966221,-0.0972573435282972,
329.081957248772));
#18224=CARTESIAN_POINT('Ctrl Pts',(32.8587891637962,0.0603374266150702,
329.081460193366));
#18225=CARTESIAN_POINT('Ctrl Pts',(32.8661917309702,0.217785364642319,329.087259510392));
#18226=CARTESIAN_POINT('Ctrl Pts',(32.8735904007249,0.375150407018542,329.093055774104));
#18227=CARTESIAN_POINT('Ctrl Pts',(32.8809890704796,0.532368399219997,329.105141794502));
#18228=CARTESIAN_POINT('Ctrl Pts',(32.8883877402344,0.688899824186392,329.123491887631));
#18229=CARTESIAN_POINT('Ctrl Pts',(32.8957851894384,0.845405426328227,329.141838953565));
#18230=CARTESIAN_POINT('Ctrl Pts',(32.9031826386425,1.0012243157115,329.166447997899));
#18231=CARTESIAN_POINT('Ctrl Pts',(32.9105800878465,1.15582151649482,329.197241415972));
#18232=CARTESIAN_POINT('Ctrl Pts',(32.9179772163099,1.31041201421304,329.228033498896));
#18233=CARTESIAN_POINT('Ctrl Pts',(32.9253743447734,1.46378056263265,329.265009349496));
#18234=CARTESIAN_POINT('Ctrl Pts',(32.9327714732369,1.61540207446399,329.308040170528));
#18235=CARTESIAN_POINT('Ctrl Pts',(32.9401697406735,1.76704693222317,329.351077617233));
#18236=CARTESIAN_POINT('Ctrl Pts',(32.9475680081102,1.91694385872561,329.40017178883));
#18237=CARTESIAN_POINT('Ctrl Pts',(32.9549662755468,2.0645827769338,329.455143958615));
#18238=CARTESIAN_POINT('Ctrl Pts',(32.9623671420726,2.21227356224677,329.510135440701));
#18239=CARTESIAN_POINT('Ctrl Pts',(32.9697680085984,2.35770441034913,329.571008902245));
#18240=CARTESIAN_POINT('Ctrl Pts',(32.9771688751241,2.50038521690832,329.63753747523));
#18241=CARTESIAN_POINT('Ctrl Pts',(32.9845778685089,2.64322270063395,329.704139102948));
#18242=CARTESIAN_POINT('Ctrl Pts',(32.9919868618937,2.78330377364729,329.776408085704));
#18243=CARTESIAN_POINT('Ctrl Pts',(32.9993958552785,2.92016229375279,329.854071246058));
#18244=CARTESIAN_POINT('Ctrl Pts',(33.0068094128587,3.05710512342743,329.931782249599));
#18245=CARTESIAN_POINT('Ctrl Pts',(33.014222970439,3.1908211281813,330.014893855699));
#18246=CARTESIAN_POINT('Ctrl Pts',(33.0216365280193,3.32087360545437,330.103089845719));
#18247=CARTESIAN_POINT('Ctrl Pts',(33.029060640156,3.45111123623795,330.191411398878));
#18248=CARTESIAN_POINT('Ctrl Pts',(33.0364847522927,3.57767462327906,330.284831571752));
#18249=CARTESIAN_POINT('Ctrl Pts',(33.0439088644294,3.7001599249798,330.382993708898));
#18250=CARTESIAN_POINT('Ctrl Pts',(33.0477659895839,3.76379597054971,330.433992891216));
#18251=CARTESIAN_POINT('Ctrl Pts',(33.0516231147384,3.82633184702468,330.486271415834));
#18252=CARTESIAN_POINT('Ctrl Pts',(33.0554802398929,3.88771497543774,330.539775472887));
#18253=CARTESIAN_POINT('Ctrl Pts',(33.0629042173309,4.00586176667684,330.642757070968));
#18254=CARTESIAN_POINT('Ctrl Pts',(33.0703281947689,4.12009214643664,330.75059164542));
#18255=CARTESIAN_POINT('Ctrl Pts',(33.0777521722069,4.22998182345058,330.862949802604));
#18256=CARTESIAN_POINT('Ctrl Pts',(33.0851673882345,4.33974181411186,330.975175360256));
#18257=CARTESIAN_POINT('Ctrl Pts',(33.0925826042622,4.44517104039266,331.091913610034));
#18258=CARTESIAN_POINT('Ctrl Pts',(33.0999978202898,4.54587822552875,331.212794998793));
#18259=CARTESIAN_POINT('Ctrl Pts',(33.1074059014339,4.64648851071844,331.33356007609));
#18260=CARTESIAN_POINT('Ctrl Pts',(33.1148139825781,4.74238556278388,331.458460071151));
#18261=CARTESIAN_POINT('Ctrl Pts',(33.1222220637222,4.83321502250708,331.587088763429));
#18262=CARTESIAN_POINT('Ctrl Pts',(33.1296246308962,4.9239768762044,331.715621715022));
#18263=CARTESIAN_POINT('Ctrl Pts',(33.1370271980702,5.00967843361043,331.847877534171));
#18264=CARTESIAN_POINT('Ctrl Pts',(33.1444297652442,5.09000577782698,331.98341720747));
#18265=CARTESIAN_POINT('Ctrl Pts',(33.1518284349989,5.17029083004798,332.118885519724));
#18266=CARTESIAN_POINT('Ctrl Pts',(33.1592271047537,5.24520711439813,332.257633922598));
#18267=CARTESIAN_POINT('Ctrl Pts',(33.1666257745084,5.31448426542388,332.399194825624));
#18268=CARTESIAN_POINT('Ctrl Pts',(33.1740232237124,5.38374998787089,332.540732375497));
#18269=CARTESIAN_POINT('Ctrl Pts',(33.1814206729164,5.44737825941084,332.685081169785));
#18270=CARTESIAN_POINT('Ctrl Pts',(33.1888181221204,5.50514483333374,332.831749339555));
#18271=CARTESIAN_POINT('Ctrl Pts',(33.1962152505839,5.5629089025987,332.97841115005));
#18272=CARTESIAN_POINT('Ctrl Pts',(33.2036123790473,5.61481164281959,333.127391788823));
#18273=CARTESIAN_POINT('Ctrl Pts',(33.2110095075108,5.66067720748356,333.278179999194));
#18274=CARTESIAN_POINT('Ctrl Pts',(33.2184077749474,5.70654983429954,333.428991427185));
#18275=CARTESIAN_POINT('Ctrl Pts',(33.225806042384,5.74638332603978,333.581610623865));
#18276=CARTESIAN_POINT('Ctrl Pts',(33.2332043098206,5.78005194584998,333.735511935297));
#18277=CARTESIAN_POINT('Ctrl Pts',(33.2406051763464,5.81373239380038,333.889467313878));
#18278=CARTESIAN_POINT('Ctrl Pts',(33.2480060428722,5.84124357803786,334.044705339639));
#18279=CARTESIAN_POINT('Ctrl Pts',(33.2554069093979,5.8625110531423,334.200691102086));
#18280=CARTESIAN_POINT('Ctrl Pts',(33.2628159027827,5.88380188196765,334.356848151814));
#18281=CARTESIAN_POINT('Ctrl Pts',(33.2702248961674,5.89883525903511,334.513754207971));
#18282=CARTESIAN_POINT('Ctrl Pts',(33.2776338895522,5.90758864879145,334.670869449655));
#18283=CARTESIAN_POINT('Ctrl Pts',(33.2850474471324,5.91634743093782,334.828081479747));
#18284=CARTESIAN_POINT('Ctrl Pts',(33.2924610047127,5.91881851105519,334.985502579854));
#18285=CARTESIAN_POINT('Ctrl Pts',(33.2998745622929,5.9150314793299,335.142594393425));
#18286=CARTESIAN_POINT('Ctrl Pts',(33.3072986744296,5.91123905607163,335.299909855953));
#18287=CARTESIAN_POINT('Ctrl Pts',(33.3147227865663,5.90117075060398,335.456894724218));
#18288=CARTESIAN_POINT('Ctrl Pts',(33.322146898703,5.88490794023595,335.613016392479));
#18289=CARTESIAN_POINT('Ctrl Pts',(33.3260040238576,5.87645875549847,335.6941278847));
#18290=CARTESIAN_POINT('Ctrl Pts',(33.3298611490122,5.86633837990226,335.775006546786));
#18291=CARTESIAN_POINT('Ctrl Pts',(33.3337182741668,5.85456360981412,335.855579044355));
#18292=CARTESIAN_POINT('Ctrl Pts',(33.3411422516047,5.83190019497317,336.010660453464));
#18293=CARTESIAN_POINT('Ctrl Pts',(33.3485662290427,5.80303641379231,336.165074692584));
#18294=CARTESIAN_POINT('Ctrl Pts',(33.3559902064807,5.76801965206156,336.31828671234));
#18295=CARTESIAN_POINT('Ctrl Pts',(33.3634054225083,5.7330442153782,336.47131791886));
#18296=CARTESIAN_POINT('Ctrl Pts',(33.370820638536,5.69193033450748,336.623149369867));
#18297=CARTESIAN_POINT('Ctrl Pts',(33.3782358545636,5.64477703226234,336.773252045972));
#18298=CARTESIAN_POINT('Ctrl Pts',(33.3856439357077,5.59766910068724,336.923210294037));
#18299=CARTESIAN_POINT('Ctrl Pts',(33.3930520168517,5.54453342766021,337.071442725081));
#18300=CARTESIAN_POINT('Ctrl Pts',(33.4004600979958,5.48551984860089,337.217431521627));
#18301=CARTESIAN_POINT('Ctrl Pts',(33.4078626651698,5.42655019442619,337.363311656046));
#18302=CARTESIAN_POINT('Ctrl Pts',(33.4152652323438,5.36171148481665,337.50695113661));
#18303=CARTESIAN_POINT('Ctrl Pts',(33.4226677995178,5.29120301706501,337.647848408558));
#18304=CARTESIAN_POINT('Ctrl Pts',(33.4300664692725,5.22073167171348,337.788671498707));
#18305=CARTESIAN_POINT('Ctrl Pts',(33.4374651390273,5.14459667982724,337.926754922663));
#18306=CARTESIAN_POINT('Ctrl Pts',(33.444863808782,5.06304493794562,338.061618284314));
#18307=CARTESIAN_POINT('Ctrl Pts',(33.452261257986,4.98150664956908,338.196459397698));
#18308=CARTESIAN_POINT('Ctrl Pts',(33.4596587071899,4.89455357762578,338.328081184006));
#18309=CARTESIAN_POINT('Ctrl Pts',(33.4670561563939,4.802477992433,338.456028890894));
#18310=CARTESIAN_POINT('Ctrl Pts',(33.4744532848574,4.71040639947719,338.583971050193));
#18311=CARTESIAN_POINT('Ctrl Pts',(33.4818504133209,4.61321295288255,338.708239143888));
#18312=CARTESIAN_POINT('Ctrl Pts',(33.4892475417843,4.51123241866238,338.82840862857));
#18313=CARTESIAN_POINT('Ctrl Pts',(33.4966458092209,4.40923618198558,338.948596616353));
#18314=CARTESIAN_POINT('Ctrl Pts',(33.5040440766575,4.30245163153557,339.064684453979));
#18315=CARTESIAN_POINT('Ctrl Pts',(33.5114423440941,4.19125275749657,339.176281945137));
#18316=CARTESIAN_POINT('Ctrl Pts',(33.5188432106198,4.08001481812373,339.287918641667));
#18317=CARTESIAN_POINT('Ctrl Pts',(33.5262440771455,3.96435973078682,339.395061586713));
#18318=CARTESIAN_POINT('Ctrl Pts',(33.5336449436713,3.84469702644138,339.497358706771));
#18319=CARTESIAN_POINT('Ctrl Pts',(33.541053937056,3.72490292100636,339.599768158848));
#18320=CARTESIAN_POINT('Ctrl Pts',(33.5484629304408,3.60109269388622,339.697320916601));
#18321=CARTESIAN_POINT('Ctrl Pts',(33.5558719238255,3.47370809671462,339.789705901339));
#18322=CARTESIAN_POINT('Ctrl Pts',(33.5632854814058,3.34624502623701,339.882147798414));
#18323=CARTESIAN_POINT('Ctrl Pts',(33.570699038986,3.21520350796785,339.969415372491));
#18324=CARTESIAN_POINT('Ctrl Pts',(33.5781125965663,3.08105227036256,340.051242170971));
#18325=CARTESIAN_POINT('Ctrl Pts',(33.5855367087029,2.94671004391106,340.133185464878));
#18326=CARTESIAN_POINT('Ctrl Pts',(33.5929608208396,2.80924958125493,340.209672332021));
#18327=CARTESIAN_POINT('Ctrl Pts',(33.6003849329763,2.66916279985474,340.280482980786));
#18328=CARTESIAN_POINT('Ctrl Pts',(33.6042420581311,2.59638207692788,340.317271963705));
#18329=CARTESIAN_POINT('Ctrl Pts',(33.6080991832859,2.52289276856279,340.352529608831));
#18330=CARTESIAN_POINT('Ctrl Pts',(33.6119563084408,2.44876563268213,340.386230355146));
#18331=CARTESIAN_POINT('Ctrl Pts',(33.6193802858788,2.30608989304925,340.451095655141));
#18332=CARTESIAN_POINT('Ctrl Pts',(33.6268042633167,2.16061981688871,340.51038589084));
#18333=CARTESIAN_POINT('Ctrl Pts',(33.6342282407547,2.012830981807,340.563851364044));
#18334=CARTESIAN_POINT('Ctrl Pts',(33.6416434567824,1.86521655978671,340.617253739946));
#18335=CARTESIAN_POINT('Ctrl Pts',(33.64905867281,1.7152891733996,340.664844910622));
#18336=CARTESIAN_POINT('Ctrl Pts',(33.6564738888376,1.56354727326193,340.706421863723));
#18337=CARTESIAN_POINT('Ctrl Pts',(33.6638819699817,1.41195137841644,340.747958811689));
#18338=CARTESIAN_POINT('Ctrl Pts',(33.6712900511258,1.25854480315241,340.783492964653));
#18339=CARTESIAN_POINT('Ctrl Pts',(33.6786981322699,1.10384407577409,340.812870101669));
#18340=CARTESIAN_POINT('Ctrl Pts',(33.6861006994439,0.94925849497255,340.842225372746));
#18341=CARTESIAN_POINT('Ctrl Pts',(33.693503266618,0.793381045138071,340.865432683527));
#18342=CARTESIAN_POINT('Ctrl Pts',(33.700905833792,0.636741345570367,340.882388207297));
#18343=CARTESIAN_POINT('Ctrl Pts',(33.7083045035467,0.480184116119897,340.899334804057));
#18344=CARTESIAN_POINT('Ctrl Pts',(33.7157031733014,0.322865806300446,340.910036129039));
#18345=CARTESIAN_POINT('Ctrl Pts',(33.7231018430562,0.165324001334266,340.914439832907));
#18346=CARTESIAN_POINT('Ctrl Pts',(33.7304992922602,0.00780818587397086,
340.918842810302));
#18347=CARTESIAN_POINT('Ctrl Pts',(33.7378967414641,-0.149930678855669,
340.91695021807));
#18348=CARTESIAN_POINT('Ctrl Pts',(33.7452941906681,-0.307352017666371,
340.90876173997));
#18349=CARTESIAN_POINT('Ctrl Pts',(33.7526913191316,-0.464766530962269,
340.900573616908));
#18350=CARTESIAN_POINT('Ctrl Pts',(33.7600884475951,-0.621863173005875,
340.886090170136));
#18351=CARTESIAN_POINT('Ctrl Pts',(33.7674855760585,-0.778103775087002,
340.865363166735));
#18352=CARTESIAN_POINT('Ctrl Pts',(33.7748838434951,-0.934368434320559,
340.844632971894));
#18353=CARTESIAN_POINT('Ctrl Pts',(33.7822821109317,-1.08977642115053,340.81765735533));
#18354=CARTESIAN_POINT('Ctrl Pts',(33.7896803783683,-1.24379722362615,340.784539655755));
#18355=CARTESIAN_POINT('Ctrl Pts',(33.7970812448941,-1.39787213522962,340.751410321583));
#18356=CARTESIAN_POINT('Ctrl Pts',(33.8044821114198,-1.55055852755869,340.712134686673));
#18357=CARTESIAN_POINT('Ctrl Pts',(33.8118829779455,-1.70133871379538,340.666866607168));
#18358=CARTESIAN_POINT('Ctrl Pts',(33.8192919713303,-1.85228447109172,340.621548818984));
#18359=CARTESIAN_POINT('Ctrl Pts',(33.8267009647151,-2.00131948440785,340.57022555242));
#18360=CARTESIAN_POINT('Ctrl Pts',(33.8341099580998,-2.14794310387718,340.513099943317));
#18361=CARTESIAN_POINT('Ctrl Pts',(33.8415235156801,-2.29465704855368,340.455939142869));
#18362=CARTESIAN_POINT('Ctrl Pts',(33.8489370732603,-2.43895629806379,340.392969026254));
#18363=CARTESIAN_POINT('Ctrl Pts',(33.8563506308406,-2.58036313086811,340.324439564438));
#18364=CARTESIAN_POINT('Ctrl Pts',(33.8637747429773,-2.72197128218691,340.255812538388));
#18365=CARTESIAN_POINT('Ctrl Pts',(33.871198855114,-2.86067846436568,340.181610535376));
#18366=CARTESIAN_POINT('Ctrl Pts',(33.8786229672507,-2.99603364518518,340.102128277437));
#18367=CARTESIAN_POINT('Ctrl Pts',(33.8824800924053,-3.06635611110962,340.060834044429));
#18368=CARTESIAN_POINT('Ctrl Pts',(33.88633721756,-3.13577429865372,340.018115252062));
#18369=CARTESIAN_POINT('Ctrl Pts',(33.8901943427146,-3.20422842184017,339.974017569648));
#18370=CARTESIAN_POINT('Ctrl Pts',(33.8976176868341,-3.33597382610674,339.88914807273));
#18371=CARTESIAN_POINT('Ctrl Pts',(33.9050410309535,-3.46454394365831,339.798912566336));
#18372=CARTESIAN_POINT('Ctrl Pts',(33.9124643750729,-3.58947148244047,339.703575771607));
#18373=CARTESIAN_POINT('Ctrl Pts',(33.9198789580572,-3.71425157998444,339.608351494704));
#18374=CARTESIAN_POINT('Ctrl Pts',(33.9272935410415,-3.83539736214807,339.508038137807));
#18375=CARTESIAN_POINT('Ctrl Pts',(33.9347081240258,-3.95246841424756,339.402944923216));
#18376=CARTESIAN_POINT('Ctrl Pts',(33.9421155730338,-4.06942682587704,339.297952824562));
#18377=CARTESIAN_POINT('Ctrl Pts',(33.9495230220418,-4.18231803652413,339.188190271556));
#18378=CARTESIAN_POINT('Ctrl Pts',(33.9569304710498,-4.29073287553002,339.074008094413));
#18379=CARTESIAN_POINT('Ctrl Pts',(33.9643324076227,-4.39906703497138,338.959910888741));
#18380=CARTESIAN_POINT('Ctrl Pts',(33.9717343441956,-4.50293119973579,338.841400877276));
#18381=CARTESIAN_POINT('Ctrl Pts',(33.9791362807685,-4.60195149056355,338.718867171734));
#18382=CARTESIAN_POINT('Ctrl Pts',(33.9865343220827,-4.70091967210267,338.596397949382));
#18383=CARTESIAN_POINT('Ctrl Pts',(33.993932363397,-4.79504882231029,338.4699095396));
#18384=CARTESIAN_POINT('Ctrl Pts',(34.0013304047112,-4.88400403846331,338.339825611432));
#18385=CARTESIAN_POINT('Ctrl Pts',(34.0087272285526,-4.97294461553028,338.209763090774));
#18386=CARTESIAN_POINT('Ctrl Pts',(34.0161240523939,-5.0567127378862,338.076106533883));
#18387=CARTESIAN_POINT('Ctrl Pts',(34.0235208762352,-5.13501564008017,337.93931028281));
#18388=CARTESIAN_POINT('Ctrl Pts',(34.0309173824593,-5.21331517997234,337.802519905724));
#18389=CARTESIAN_POINT('Ctrl Pts',(34.0383138886833,-5.28614978086938,337.66259042648));
#18390=CARTESIAN_POINT('Ctrl Pts',(34.0457103949074,-5.35327177774928,337.520002348422));
#18391=CARTESIAN_POINT('Ctrl Pts',(34.0531080437924,-5.420404144077,337.377392242419));
#18392=CARTESIAN_POINT('Ctrl Pts',(34.0605056926775,-5.48182199018751,337.232123057568));
#18393=CARTESIAN_POINT('Ctrl Pts',(34.0679033415625,-5.53732516275085,337.084696765591));
#18394=CARTESIAN_POINT('Ctrl Pts',(34.0753035937919,-5.59284786771878,336.937218592076));
#18395=CARTESIAN_POINT('Ctrl Pts',(34.0827038460213,-5.6424516235287,336.787582149161));
#18396=CARTESIAN_POINT('Ctrl Pts',(34.0901040982507,-5.68598569908107,336.636305959271));
#18397=CARTESIAN_POINT('Ctrl Pts',(34.0975124774253,-5.72956758368598,336.484863638109));
#18398=CARTESIAN_POINT('Ctrl Pts',(34.1049208565999,-5.76706637302287,336.331778332696));
#18399=CARTESIAN_POINT('Ctrl Pts',(34.1123292357745,-5.79838199679146,336.177580902437));
#18400=CARTESIAN_POINT('Ctrl Pts',(34.1197421840418,-5.82971693436465,336.023288371437));
#18401=CARTESIAN_POINT('Ctrl Pts',(34.1271551323091,-5.85486104813616,335.867882716476));
#18402=CARTESIAN_POINT('Ctrl Pts',(34.1345680805764,-5.87376606042453,335.711900856795));
#18403=CARTESIAN_POINT('Ctrl Pts',(34.1419915729434,-5.89269796300362,335.555697130156));
#18404=CARTESIAN_POINT('Ctrl Pts',(34.1494150653104,-5.90537301024448,335.398915932984));
#18405=CARTESIAN_POINT('Ctrl Pts',(34.1568385576774,-5.91179499930531,335.242095949344));
#18406=CARTESIAN_POINT('Ctrl Pts',(34.1606595785391,-5.91510052626779,335.161377548975));
#18407=CARTESIAN_POINT('Ctrl Pts',(34.1644805994007,-5.91675023582117,335.080648829086));
#18408=CARTESIAN_POINT('Ctrl Pts',(34.1683016202624,-5.91674999997471,334.999982700985));
#18409=CARTESIAN_POINT('',(35.9183016044877,-5.91463655468594,335.005215113745));
#18410=CARTESIAN_POINT('Ctrl Pts',(34.1683016202945,-5.91674999997471,334.999982700307));
#18411=CARTESIAN_POINT('Ctrl Pts',(34.1757262328824,-5.9167495416843,334.843240622263));
#18412=CARTESIAN_POINT('Ctrl Pts',(34.1831508454702,-5.91051634278605,334.686262312169));
#18413=CARTESIAN_POINT('Ctrl Pts',(34.1905754580581,-5.89801996188907,334.529584129033));
#18414=CARTESIAN_POINT('Ctrl Pts',(34.1979913089862,-5.88553832775989,334.373090839171));
#18415=CARTESIAN_POINT('Ctrl Pts',(34.2054071599143,-5.86680825310907,334.216897339617));
#18416=CARTESIAN_POINT('Ctrl Pts',(34.2128230108424,-5.8418512629109,334.06154148492));
#18417=CARTESIAN_POINT('Ctrl Pts',(34.2202317260019,-5.81691828712562,333.906335118587));
#18418=CARTESIAN_POINT('Ctrl Pts',(34.2276404411614,-5.78577038304834,333.751965158449));
#18419=CARTESIAN_POINT('Ctrl Pts',(34.235049156321,-5.74848097373168,333.598965718783));
#18420=CARTESIAN_POINT('Ctrl Pts',(34.2424523559939,-5.7112193248611,333.446080180967));
#18421=CARTESIAN_POINT('Ctrl Pts',(34.2498555556667,-5.66782536247198,333.294563493033));
#18422=CARTESIAN_POINT('Ctrl Pts',(34.2572587553396,-5.61842380275774,333.144940827061));
#18423=CARTESIAN_POINT('Ctrl Pts',(34.2646580554474,-5.56904826484596,332.995396973407));
#18424=CARTESIAN_POINT('Ctrl Pts',(34.2720573555553,-5.5136715484983,332.847745508246));
#18425=CARTESIAN_POINT('Ctrl Pts',(34.2794566556631,-5.45246852796488,332.70249754863));
#18426=CARTESIAN_POINT('Ctrl Pts',(34.286854732152,-5.39127562854728,332.557273608603));
#18427=CARTESIAN_POINT('Ctrl Pts',(34.2942528086408,-5.32425848194353,332.414452728791));
#18428=CARTESIAN_POINT('Ctrl Pts',(34.3016508851297,-5.25164056712346,332.274527212346));
#18429=CARTESIAN_POINT('Ctrl Pts',(34.3090486377602,-5.17902583122722,332.134607821284));
#18430=CARTESIAN_POINT('Ctrl Pts',(34.3164463903907,-5.10081098649808,331.997583872765));
#18431=CARTESIAN_POINT('Ctrl Pts',(34.3238441430212,-5.01726592936693,331.863923923672));
#18432=CARTESIAN_POINT('Ctrl Pts',(34.331243030939,-4.93370805109248,331.730243462614));
#18433=CARTESIAN_POINT('Ctrl Pts',(34.3386419188568,-4.84481852946019,331.599928345348));
#18434=CARTESIAN_POINT('Ctrl Pts',(34.3460408067747,-4.75091104020307,331.473418815541));
#18435=CARTESIAN_POINT('Ctrl Pts',(34.3534422895252,-4.65697061704751,331.346864918113));
#18436=CARTESIAN_POINT('Ctrl Pts',(34.3608437722757,-4.55800894469779,331.224119564853));
#18437=CARTESIAN_POINT('Ctrl Pts',(34.3682452550263,-4.45438038023647,331.105590418219));
#18438=CARTESIAN_POINT('Ctrl Pts',(34.3756548645294,-4.35063803266724,330.986931127791));
#18439=CARTESIAN_POINT('Ctrl Pts',(34.3830644740325,-4.24221880538197,330.872497570185));
#18440=CARTESIAN_POINT('Ctrl Pts',(34.3904740835357,-4.12951486858929,330.762661506016));
#18441=CARTESIAN_POINT('Ctrl Pts',(34.3978882523305,-4.01674158264789,330.652757857361));
#18442=CARTESIAN_POINT('Ctrl Pts',(34.4053024211252,-3.89967861042304,330.547457588168));
#18443=CARTESIAN_POINT('Ctrl Pts',(34.41271658992,-3.7787512719973,330.447092205318));
#18444=CARTESIAN_POINT('Ctrl Pts',(34.4201413236992,-3.65765161547493,330.346583804586));
#18445=CARTESIAN_POINT('Ctrl Pts',(34.4275660574785,-3.53267689047145,330.251024560831));
#18446=CARTESIAN_POINT('Ctrl Pts',(34.4349907912577,-3.40428211726297,330.160703167961));
#18447=CARTESIAN_POINT('Ctrl Pts',(34.438883997926,-3.33695749632928,330.11334256764));
#18448=CARTESIAN_POINT('Ctrl Pts',(34.4427772045943,-3.26869296821449,330.067421359335));
#18449=CARTESIAN_POINT('Ctrl Pts',(34.4466704112625,-3.19955672855037,330.022976059603));
#18450=CARTESIAN_POINT('Ctrl Pts',(34.4540943887005,-3.06772044880581,329.938223070472));
#18451=CARTESIAN_POINT('Ctrl Pts',(34.4615183661385,-2.93231543183702,329.858584157325));
#18452=CARTESIAN_POINT('Ctrl Pts',(34.4689423435766,-2.79377629797551,329.784374959857));
#18453=CARTESIAN_POINT('Ctrl Pts',(34.4763575596042,-2.65540066113629,329.710253340407));
#18454=CARTESIAN_POINT('Ctrl Pts',(34.4837727756319,-2.51389859557135,329.641548856155));
#18455=CARTESIAN_POINT('Ctrl Pts',(34.4911879916595,-2.3697340849914,329.578534245342));
#18456=CARTESIAN_POINT('Ctrl Pts',(34.4985960728037,-2.22570828877776,329.51558026687));
#18457=CARTESIAN_POINT('Ctrl Pts',(34.5060041539477,-2.07902548728249,329.458305411071));
#18458=CARTESIAN_POINT('Ctrl Pts',(34.5134122350919,-1.93017458584001,329.406936739972));
#18459=CARTESIAN_POINT('Ctrl Pts',(34.5208148022659,-1.78143447684204,329.355606303512));
#18460=CARTESIAN_POINT('Ctrl Pts',(34.52821736944,-1.63052983240379,329.310173419742));
#18461=CARTESIAN_POINT('Ctrl Pts',(34.535619936614,-1.4779697758931,329.270817169609));
#18462=CARTESIAN_POINT('Ctrl Pts',(34.5430186063688,-1.32549004158496,329.231481640369));
#18463=CARTESIAN_POINT('Ctrl Pts',(34.5504172761236,-1.17135699145214,329.19821646612));
#18464=CARTESIAN_POINT('Ctrl Pts',(34.5578159458784,-1.01609505146479,329.171150936172));
#18465=CARTESIAN_POINT('Ctrl Pts',(34.5652133950824,-0.860858724876622,
329.144089871196));
#18466=CARTESIAN_POINT('Ctrl Pts',(34.5726108442863,-0.704494245353079,
329.123226484724));
#18467=CARTESIAN_POINT('Ctrl Pts',(34.5800082934903,-0.547536497570136,
329.108639007298));
#18468=CARTESIAN_POINT('Ctrl Pts',(34.5874054219538,-0.3905855552015,329.09405216236));
#18469=CARTESIAN_POINT('Ctrl Pts',(34.5948025504173,-0.23304176732925,329.085740719956));
#18470=CARTESIAN_POINT('Ctrl Pts',(34.6021996788808,-0.0754451444839536,
329.083731024313));
#18471=CARTESIAN_POINT('Ctrl Pts',(34.6095979463175,0.0821757443071198,
329.081721019228));
#18472=CARTESIAN_POINT('Ctrl Pts',(34.6169962137541,0.239849111065977,329.086014697681));
#18473=CARTESIAN_POINT('Ctrl Pts',(34.6243944811907,0.397035088618084,329.096586267175));
#18474=CARTESIAN_POINT('Ctrl Pts',(34.6317953477165,0.55427628725711,329.107161550572));
#18475=CARTESIAN_POINT('Ctrl Pts',(34.6391962142422,0.711029383645316,329.124019091107));
#18476=CARTESIAN_POINT('Ctrl Pts',(34.646597080768,0.866759920317203,329.14708125778));
#18477=CARTESIAN_POINT('Ctrl Pts',(34.6540060741528,1.02266146400678,329.170168748917));
#18478=CARTESIAN_POINT('Ctrl Pts',(34.6614150675375,1.17753783614681,329.199474417956));
#18479=CARTESIAN_POINT('Ctrl Pts',(34.6688240609223,1.33086433522249,329.234869413124));
#18480=CARTESIAN_POINT('Ctrl Pts',(34.6762376185026,1.48428528871039,329.27028621283));
#18481=CARTESIAN_POINT('Ctrl Pts',(34.6836511760828,1.63615410745543,329.311799715318));
#18482=CARTESIAN_POINT('Ctrl Pts',(34.6910647336631,1.78596202810581,329.359231417913));
#18483=CARTESIAN_POINT('Ctrl Pts',(34.6984888457998,1.93598322775725,329.406730648219));
#18484=CARTESIAN_POINT('Ctrl Pts',(34.7059129579365,2.083937319324,329.460164779894));
#18485=CARTESIAN_POINT('Ctrl Pts',(34.7133370700733,2.22933549972864,329.519307179548));
#18486=CARTESIAN_POINT('Ctrl Pts',(34.7171941952277,2.30487570827037,329.550034037279));
#18487=CARTESIAN_POINT('Ctrl Pts',(34.7210513203821,2.37972641491085,329.582300919648));
#18488=CARTESIAN_POINT('Ctrl Pts',(34.7249084455365,2.4538218752867,329.616071251691));
#18489=CARTESIAN_POINT('Ctrl Pts',(34.7323324229745,2.59643664770587,329.681070486388));
#18490=CARTESIAN_POINT('Ctrl Pts',(34.7397564004125,2.73668213301252,329.751838268312));
#18491=CARTESIAN_POINT('Ctrl Pts',(34.7471803778505,2.87405770505323,329.828179926706));
#18492=CARTESIAN_POINT('Ctrl Pts',(34.7545955938781,3.01127115324966,329.904431490457));
#18493=CARTESIAN_POINT('Ctrl Pts',(34.7620108099058,3.14562110686627,329.986243657513));
#18494=CARTESIAN_POINT('Ctrl Pts',(34.7694260259334,3.27662712628925,330.073373848386));
#18495=CARTESIAN_POINT('Ctrl Pts',(34.7768341070775,3.40750709238005,330.160420203028));
#18496=CARTESIAN_POINT('Ctrl Pts',(34.7842421882216,3.53504922107281,330.252774189242));
#18497=CARTESIAN_POINT('Ctrl Pts',(34.7916502693657,3.65879799633629,330.350147552394));
#18498=CARTESIAN_POINT('Ctrl Pts',(34.7990528365397,3.78245466312607,330.447448438773));
#18499=CARTESIAN_POINT('Ctrl Pts',(34.8064554037137,3.90232330636831,330.549761033344));
#18500=CARTESIAN_POINT('Ctrl Pts',(34.8138579708877,4.01797781720591,330.656754114382));
#18501=CARTESIAN_POINT('Ctrl Pts',(34.8212566406425,4.13357143644902,330.763690864029));
#18502=CARTESIAN_POINT('Ctrl Pts',(34.8286553103972,4.2449550687353,330.875302939628));
#18503=CARTESIAN_POINT('Ctrl Pts',(34.8360539801519,4.3517361949416,330.991219306056));
#18504=CARTESIAN_POINT('Ctrl Pts',(34.8434514293559,4.45849970557797,331.107116549883));
#18505=CARTESIAN_POINT('Ctrl Pts',(34.8508488785599,4.56066196442487,331.227316401044));
#18506=CARTESIAN_POINT('Ctrl Pts',(34.8582463277639,4.65786772896121,331.351411398636));
#18507=CARTESIAN_POINT('Ctrl Pts',(34.8656434562274,4.75506927882492,331.475501015686));
#18508=CARTESIAN_POINT('Ctrl Pts',(34.8730405846908,4.84731453153763,331.603485149561));
#18509=CARTESIAN_POINT('Ctrl Pts',(34.8804377131543,4.93428910299219,331.734923950259));
#18510=CARTESIAN_POINT('Ctrl Pts',(34.8878359805909,5.0212770663597,331.866382989251));
#18511=CARTESIAN_POINT('Ctrl Pts',(34.8952342480275,5.10299252659552,332.001297442955));
#18512=CARTESIAN_POINT('Ctrl Pts',(34.9026325154641,5.17916502005664,332.139199367743));
#18513=CARTESIAN_POINT('Ctrl Pts',(34.9100333819899,5.25536427371587,332.277149738928));
#18514=CARTESIAN_POINT('Ctrl Pts',(34.9174342485157,5.32601650318714,332.41808934433));
#18515=CARTESIAN_POINT('Ctrl Pts',(34.9248351150414,5.39089776443169,332.561526736676));
#18516=CARTESIAN_POINT('Ctrl Pts',(34.9322441084262,5.45585027150397,332.705121636992));
#18517=CARTESIAN_POINT('Ctrl Pts',(34.939653101811,5.51501900096914,332.851219461543));
#18518=CARTESIAN_POINT('Ctrl Pts',(34.9470620951958,5.56822836093612,332.999309248543));
#18519=CARTESIAN_POINT('Ctrl Pts',(34.954475652776,5.62147049970415,333.147490263959));
#18520=CARTESIAN_POINT('Ctrl Pts',(34.9618892103563,5.66874584186422,333.297665331861));
#18521=CARTESIAN_POINT('Ctrl Pts',(34.9693027679365,5.70992917308212,333.449310024252));
#18522=CARTESIAN_POINT('Ctrl Pts',(34.9767268800732,5.75117113631163,333.601170610625));
#18523=CARTESIAN_POINT('Ctrl Pts',(34.9841509922099,5.78630368357058,333.754504637383));
#18524=CARTESIAN_POINT('Ctrl Pts',(34.9915751043466,5.81525287631618,333.908778415263));
#18525=CARTESIAN_POINT('Ctrl Pts',(34.9954322295012,5.83029314746079,333.988929854033));
#18526=CARTESIAN_POINT('Ctrl Pts',(34.9992893546558,5.84366524998968,334.069334871644));
#18527=CARTESIAN_POINT('Ctrl Pts',(35.0031464798104,5.85536436252227,334.149918389445));
#18528=CARTESIAN_POINT('Ctrl Pts',(35.0105704572484,5.87788215595793,334.305021009674));
#18529=CARTESIAN_POINT('Ctrl Pts',(35.0179944346864,5.89426689775692,334.461252937728));
#18530=CARTESIAN_POINT('Ctrl Pts',(35.0254184121243,5.90441137317563,334.618087838876));
#18531=CARTESIAN_POINT('Ctrl Pts',(35.032833628152,5.91454387658704,334.774737651244));
#18532=CARTESIAN_POINT('Ctrl Pts',(35.0402488441796,5.91845074882391,334.931988651446));
#18533=CARTESIAN_POINT('Ctrl Pts',(35.0476640602072,5.91607598671165,335.08930555388));
#18534=CARTESIAN_POINT('Ctrl Pts',(35.0550721413513,5.91370350958354,335.246471086782));
#18535=CARTESIAN_POINT('Ctrl Pts',(35.0624802224953,5.90506143649155,335.403702025002));
#18536=CARTESIAN_POINT('Ctrl Pts',(35.0698883036394,5.89014566104608,335.560459324269));
#18537=CARTESIAN_POINT('Ctrl Pts',(35.0772908708134,5.8752409876847,335.717099946215));
#18538=CARTESIAN_POINT('Ctrl Pts',(35.0846934379874,5.85407194508644,335.87326726122));
#18539=CARTESIAN_POINT('Ctrl Pts',(35.0920960051614,5.82668647271372,336.028423702175));
#18540=CARTESIAN_POINT('Ctrl Pts',(35.0994946749162,5.79931541867251,336.183498453942));
#18541=CARTESIAN_POINT('Ctrl Pts',(35.1068933446709,5.76573451778398,336.337563025003));
#18542=CARTESIAN_POINT('Ctrl Pts',(35.1142920144256,5.72604336677771,336.490086549258));
#18543=CARTESIAN_POINT('Ctrl Pts',(35.1216894636295,5.68635876357889,336.642584911869));
#18544=CARTESIAN_POINT('Ctrl Pts',(35.1290869128335,5.64056600471861,336.793542371398));
#18545=CARTESIAN_POINT('Ctrl Pts',(35.1364843620374,5.58881549064892,336.942439696357));
#18546=CARTESIAN_POINT('Ctrl Pts',(35.1438814905009,5.53706722039129,337.091330565387));
#18547=CARTESIAN_POINT('Ctrl Pts',(35.1512786189643,5.47936183106871,337.238161124927));
#18548=CARTESIAN_POINT('Ctrl Pts',(35.1586757474278,5.41589907065227,337.382428974599));
#18549=CARTESIAN_POINT('Ctrl Pts',(35.1660740148644,5.35242653855487,337.526719037918));
#18550=CARTESIAN_POINT('Ctrl Pts',(35.173472282301,5.28319502052826,337.668445264042));
#18551=CARTESIAN_POINT('Ctrl Pts',(35.1808705497376,5.20845165695409,337.807126983176));
#18552=CARTESIAN_POINT('Ctrl Pts',(35.1882714162633,5.13368203525028,337.945857422656));
#18553=CARTESIAN_POINT('Ctrl Pts',(35.1956722827891,5.05339688964474,338.081540897313));
#18554=CARTESIAN_POINT('Ctrl Pts',(35.2030731493149,4.96788829966441,338.213723137509));
#18555=CARTESIAN_POINT('Ctrl Pts',(35.2104821426996,4.88228581307733,338.346050526441));
#18556=CARTESIAN_POINT('Ctrl Pts',(35.2178911360843,4.79144863016722,338.474868689313));
#18557=CARTESIAN_POINT('Ctrl Pts',(35.225300129469,4.69571140675345,338.599753456417));
#18558=CARTESIAN_POINT('Ctrl Pts',(35.2327136870493,4.59991520590759,338.724715156845));
#18559=CARTESIAN_POINT('Ctrl Pts',(35.2401272446295,4.499213187766,338.845738346928));
#18560=CARTESIAN_POINT('Ctrl Pts',(35.2475408022098,4.39397859435842,338.96243393318));
#18561=CARTESIAN_POINT('Ctrl Pts',(35.2549649143464,4.2885941802415,339.079295656964));
#18562=CARTESIAN_POINT('Ctrl Pts',(35.2623890264831,4.1786645631295,339.191817205658));
#18563=CARTESIAN_POINT('Ctrl Pts',(35.2698131386198,4.06459852132363,339.299647592879));
#18564=CARTESIAN_POINT('Ctrl Pts',(35.2736702637746,4.00533662022828,339.355669820367));
#18565=CARTESIAN_POINT('Ctrl Pts',(35.2775273889295,3.94495873751914,339.410426475336));
#18566=CARTESIAN_POINT('Ctrl Pts',(35.2813845140844,3.88352539930828,339.463872874022));
#18567=CARTESIAN_POINT('Ctrl Pts',(35.2888084915224,3.7652819670866,339.566743494511));
#18568=CARTESIAN_POINT('Ctrl Pts',(35.2962324689603,3.64276992966733,339.665067834299));
#18569=CARTESIAN_POINT('Ctrl Pts',(35.3036564463983,3.51637387310443,339.758470904298));
#18570=CARTESIAN_POINT('Ctrl Pts',(35.311071662426,3.39012698290558,339.851763744621));
#18571=CARTESIAN_POINT('Ctrl Pts',(35.3184868784536,3.26000549477615,339.940146656104));
#18572=CARTESIAN_POINT('Ctrl Pts',(35.3259020944813,3.12642923526749,340.02328287073));
#18573=CARTESIAN_POINT('Ctrl Pts',(35.3333101756254,2.99298150216326,340.106339092108));
#18574=CARTESIAN_POINT('Ctrl Pts',(35.3407182567695,2.85608593020623,340.184158471055));
#18575=CARTESIAN_POINT('Ctrl Pts',(35.3481263379136,2.71619359102158,340.256445846634));
#18576=CARTESIAN_POINT('Ctrl Pts',(35.3555289050876,2.57640537625973,340.328679417399));
#18577=CARTESIAN_POINT('Ctrl Pts',(35.3629314722616,2.43362516575836,340.395389012884));
#18578=CARTESIAN_POINT('Ctrl Pts',(35.3703340394356,2.28833095396235,340.456324037998));
#18579=CARTESIAN_POINT('Ctrl Pts',(35.3777327091904,2.14311323893425,340.517226981088));
#18580=CARTESIAN_POINT('Ctrl Pts',(35.3851313789451,1.99538450196292,340.572361264737));
#18581=CARTESIAN_POINT('Ctrl Pts',(35.3925300486998,1.84564505718196,340.621523359855));
#18582=CARTESIAN_POINT('Ctrl Pts',(35.3999274979038,1.69593031475931,340.670677344754));
#18583=CARTESIAN_POINT('Ctrl Pts',(35.4073249471078,1.54420587709747,340.713860980171));
#18584=CARTESIAN_POINT('Ctrl Pts',(35.4147223963118,1.39098976734667,340.750919755103));
#18585=CARTESIAN_POINT('Ctrl Pts',(35.4221195247753,1.23778030077949,340.787976923231));
#18586=CARTESIAN_POINT('Ctrl Pts',(35.4295166532388,1.08307965347235,340.818909671162));
#18587=CARTESIAN_POINT('Ctrl Pts',(35.4369137817022,0.927418399709803,340.843614093554));
#18588=CARTESIAN_POINT('Ctrl Pts',(35.4443120491388,0.771733177999778,340.86832231981));
#18589=CARTESIAN_POINT('Ctrl Pts',(35.4517103165754,0.615087423947733,340.886800252516));
#18590=CARTESIAN_POINT('Ctrl Pts',(35.459108584012,0.458019084879539,340.898995599285));
#18591=CARTESIAN_POINT('Ctrl Pts',(35.4665094505378,0.300895566052063,340.911195230408));
#18592=CARTESIAN_POINT('Ctrl Pts',(35.4739103170636,0.143349538484667,340.917107852313));
#18593=CARTESIAN_POINT('Ctrl Pts',(35.4813111835893,-0.0140789318007903,
340.916733249537));
#18594=CARTESIAN_POINT('Ctrl Pts',(35.4887201769741,-0.1716802735976,340.916358235412));
#18595=CARTESIAN_POINT('Ctrl Pts',(35.4961291703589,-0.329163426881736,
340.909682209891));
#18596=CARTESIAN_POINT('Ctrl Pts',(35.5035381637436,-0.485990596829314,
340.896757049624));
#18597=CARTESIAN_POINT('Ctrl Pts',(35.5109517213239,-0.642914377722902,
340.883823927013));
#18598=CARTESIAN_POINT('Ctrl Pts',(35.5183652789041,-0.799181000477436,
340.864634044037));
#18599=CARTESIAN_POINT('Ctrl Pts',(35.5257788364844,-0.954261285400897,
340.839290707071));
#18600=CARTESIAN_POINT('Ctrl Pts',(35.5332029486211,-1.10956235550119,340.813911289225));
#18601=CARTESIAN_POINT('Ctrl Pts',(35.5406270607577,-1.26367334991961,340.782360995433));
#18602=CARTESIAN_POINT('Ctrl Pts',(35.5480511728944,-1.41607790332439,340.744793637218));
#18603=CARTESIAN_POINT('Ctrl Pts',(35.551908298049,-1.49525820472476,340.725275882138));
#18604=CARTESIAN_POINT('Ctrl Pts',(35.5557654232037,-1.57397818088169,340.704134800404));
#18605=CARTESIAN_POINT('Ctrl Pts',(35.5596225483583,-1.65216750211017,340.681397108764));
#18606=CARTESIAN_POINT('Ctrl Pts',(35.5670465257963,-1.80266190750961,340.637632879457));
#18607=CARTESIAN_POINT('Ctrl Pts',(35.5744705032343,-1.95164323568219,340.587818835621));
#18608=CARTESIAN_POINT('Ctrl Pts',(35.5818944806723,-2.09858802872165,340.532075455759));
#18609=CARTESIAN_POINT('Ctrl Pts',(35.5893096966999,-2.24535940479629,340.476397861472));
#18610=CARTESIAN_POINT('Ctrl Pts',(35.5967249127276,-2.39009868422559,340.414804990898));
#18611=CARTESIAN_POINT('Ctrl Pts',(35.6041401287552,-2.53229547936181,340.347467640641));
#18612=CARTESIAN_POINT('Ctrl Pts',(35.6115482098993,-2.67435545345782,340.280195082044));
#18613=CARTESIAN_POINT('Ctrl Pts',(35.6189562910435,-2.81387747847031,340.207189206269));
#18614=CARTESIAN_POINT('Ctrl Pts',(35.6263643721876,-2.95036924653195,340.128669600551));
#18615=CARTESIAN_POINT('Ctrl Pts',(35.6337669393616,-3.08675942127778,340.05020843841));
#18616=CARTESIAN_POINT('Ctrl Pts',(35.6411695065356,-3.22012350793736,339.96624190323));
#18617=CARTESIAN_POINT('Ctrl Pts',(35.6485720737096,-3.34999210553022,339.877036339355));
#18618=CARTESIAN_POINT('Ctrl Pts',(35.6559707434644,-3.47979232787402,339.787877741819));
#18619=CARTESIAN_POINT('Ctrl Pts',(35.6633694132191,-3.60610041948226,339.693485819732));
#18620=CARTESIAN_POINT('Ctrl Pts',(35.6707680829739,-3.72847447971309,339.594171156654));
#18621=CARTESIAN_POINT('Ctrl Pts',(35.6781655321779,-3.85082835202389,339.49487287741));
#18622=CARTESIAN_POINT('Ctrl Pts',(35.6855629813819,-3.96924919149363,339.390653703882));
#18623=CARTESIAN_POINT('Ctrl Pts',(35.6929604305859,-4.08332673447283,339.281865638018));
#18624=CARTESIAN_POINT('Ctrl Pts',(35.7003575590493,-4.19739933124848,339.173082289015));
#18625=CARTESIAN_POINT('Ctrl Pts',(35.7077546875128,-4.3071287358838,339.059730699127));
#18626=CARTESIAN_POINT('Ctrl Pts',(35.7151518159763,-4.41214044797045,338.942200810446));
#18627=CARTESIAN_POINT('Ctrl Pts',(35.7225500834129,-4.51716832923962,338.824652825096));
#18628=CARTESIAN_POINT('Ctrl Pts',(35.7299483508495,-4.61747682291074,338.702925538274));
#18629=CARTESIAN_POINT('Ctrl Pts',(35.7373466182861,-4.71273084103459,338.577443022951));
#18630=CARTESIAN_POINT('Ctrl Pts',(35.7447474848119,-4.80801832289658,338.451916424301));
#18631=CARTESIAN_POINT('Ctrl Pts',(35.7521483513377,-4.89824756830224,338.322632267601));
#18632=CARTESIAN_POINT('Ctrl Pts',(35.7595492178634,-4.98312613535172,338.190044589293));
#18633=CARTESIAN_POINT('Ctrl Pts',(35.7669582112482,-5.06809790718252,338.057311317037));
#18634=CARTESIAN_POINT('Ctrl Pts',(35.7743672046329,-5.14770706551855,337.921267593205));
#18635=CARTESIAN_POINT('Ctrl Pts',(35.7817761980177,-5.22170620290343,337.78239373437));
#18636=CARTESIAN_POINT('Ctrl Pts',(35.7891897555979,-5.29575092630956,337.643434324447));
#18637=CARTESIAN_POINT('Ctrl Pts',(35.7966033131782,-5.3641785804664,337.501641640776));
#18638=CARTESIAN_POINT('Ctrl Pts',(35.8040168707585,-5.42678966841234,337.357516586859));
#18639=CARTESIAN_POINT('Ctrl Pts',(35.8114409828952,-5.48948989470437,337.213186344541));
#18640=CARTESIAN_POINT('Ctrl Pts',(35.8188650950318,-5.54635688152531,337.066517447194));
#18641=CARTESIAN_POINT('Ctrl Pts',(35.8262892071685,-5.59724053735629,336.918027353683));
#18642=CARTESIAN_POINT('Ctrl Pts',(35.8301463323231,-5.62367664516925,336.840880771797));
#18643=CARTESIAN_POINT('Ctrl Pts',(35.8340034574776,-5.64849855456325,336.763242812029));
#18644=CARTESIAN_POINT('Ctrl Pts',(35.8378605826322,-5.67169067279419,336.685187074078));
#18645=CARTESIAN_POINT('Ctrl Pts',(35.8470348007207,-5.72685340204471,336.499530572323));
#18646=CARTESIAN_POINT('Ctrl Pts',(35.8562090188092,-5.77292764653191,336.311058344617));
#18647=CARTESIAN_POINT('Ctrl Pts',(35.8653832368978,-5.80966959513859,336.120566712794));
#18648=CARTESIAN_POINT('Ctrl Pts',(35.8744336397492,-5.84591567444786,335.932645955822));
#18649=CARTESIAN_POINT('Ctrl Pts',(35.8834840426007,-5.87307965956882,335.742759892796));
#18650=CARTESIAN_POINT('Ctrl Pts',(35.8925344454522,-5.89097312716808,335.551693916482));
#18651=CARTESIAN_POINT('Ctrl Pts',(35.9011234889216,-5.90795444540889,335.370367847023));
#18652=CARTESIAN_POINT('Ctrl Pts',(35.9097125323909,-5.91658653424087,335.187979188446));
#18653=CARTESIAN_POINT('Ctrl Pts',(35.9183015758603,-5.91674769948109,335.005217584232));
#18654=CARTESIAN_POINT('',(37.6683016202945,-5.907956964761,334.997521372297));
#18655=CARTESIAN_POINT('Ctrl Pts',(35.9183016202945,-5.91347087048126,335.005213749647));
#18656=CARTESIAN_POINT('Ctrl Pts',(35.9842339524984,-5.9016480507818,333.603040816822));
#18657=CARTESIAN_POINT('Ctrl Pts',(36.1429122961271,-4.70094670253729,330.210249656623));
#18658=CARTESIAN_POINT('Ctrl Pts',(36.3943366511801,0.96493722398234,328.070243938278));
#18659=CARTESIAN_POINT('Ctrl Pts',(36.672574685454,6.34956261214914,332.061347663363));
#18660=CARTESIAN_POINT('Ctrl Pts',(36.9508127197281,5.90728811053532,338.749209263345));
#18661=CARTESIAN_POINT('Ctrl Pts',(37.2290507540018,0.043982501314167,341.996476860591));
#18662=CARTESIAN_POINT('Ctrl Pts',(37.4682137208575,-5.03058858133461,339.268830814406));
#18663=CARTESIAN_POINT('Ctrl Pts',(37.6146306762883,-5.9036517049508,336.141614378199));
#18664=CARTESIAN_POINT('Ctrl Pts',(37.6683016202945,-5.907956964761,334.997521372297));
#18665=CARTESIAN_POINT('',(39.4183016202944,-5.92257269867875,334.995813786999));
#18666=CARTESIAN_POINT('Ctrl Pts',(37.6683016202945,-5.907956964761,334.997521372297));
#18667=CARTESIAN_POINT('Ctrl Pts',(37.7073766877129,-5.91109140408291,334.164565810094));
#18668=CARTESIAN_POINT('Ctrl Pts',(37.8391977665561,-5.35709580127298,331.358543580458));
#18669=CARTESIAN_POINT('Ctrl Pts',(38.0637648568237,-1.05198365643141,328.082923066223));
#18670=CARTESIAN_POINT('Ctrl Pts',(38.3420028910976,5.24742884367505,330.372137269561));
#18671=CARTESIAN_POINT('Ctrl Pts',(38.6202409253717,6.73135334586379,336.908272793485));
#18672=CARTESIAN_POINT('Ctrl Pts',(38.8984789596455,2.03801423716468,341.693214540886));
#18673=CARTESIAN_POINT('Ctrl Pts',(39.1644991912865,-4.23736427179148,340.395493932002));
#18674=CARTESIAN_POINT('Ctrl Pts',(39.3377734115028,-5.90889301881075,336.701643735705));
#18675=CARTESIAN_POINT('Ctrl Pts',(39.4183016202944,-5.92257269867875,334.995813786999));
#18676=CARTESIAN_POINT('',(41.1683016202944,-5.92116599764251,335.0047121213));
#18677=CARTESIAN_POINT('Ctrl Pts',(39.4183016202944,-5.92257269867875,334.995813786999));
#18678=CARTESIAN_POINT('Ctrl Pts',(39.4305194229274,-5.9246481903756,334.737003936992));
#18679=CARTESIAN_POINT('Ctrl Pts',(39.5354832369853,-5.79155819114906,332.515703125699));
#18680=CARTESIAN_POINT('Ctrl Pts',(39.7331930624671,-2.98148109258298,328.67043497421));
#18681=CARTESIAN_POINT('Ctrl Pts',(40.0114310967413,3.70921576899493,329.067518116311));
#18682=CARTESIAN_POINT('Ctrl Pts',(40.2896691310152,6.99602006730123,334.908752319798));
#18683=CARTESIAN_POINT('Ctrl Pts',(40.5679071652891,3.86268001093083,340.833723172585));
#18684=CARTESIAN_POINT('Ctrl Pts',(40.8461451995632,-2.81538447840677,341.405172375509));
#18685=CARTESIAN_POINT('Ctrl Pts',(41.0462766845649,-5.76043079342616,337.58831708874));
#18686=CARTESIAN_POINT('Ctrl Pts',(41.153662158142,-5.92386532355179,335.315011839286));
#18687=CARTESIAN_POINT('Ctrl Pts',(41.1683016202944,-5.92116599764251,335.0047121213));
#18688=CARTESIAN_POINT('',(42.9183016202944,-5.90741276477635,335.001689847821));
#18689=CARTESIAN_POINT('Ctrl Pts',(41.1683016202944,-5.92116599764251,335.0047121213));
#18690=CARTESIAN_POINT('Ctrl Pts',(41.2464081695666,-5.90676416853575,333.349156749142));
#18691=CARTESIAN_POINT('Ctrl Pts',(41.4172607302634,-4.31984453201313,329.703557399639));
#18692=CARTESIAN_POINT('Ctrl Pts',(41.6808593023849,1.86275416207226,328.255908522793));
#18693=CARTESIAN_POINT('Ctrl Pts',(41.9590973366588,6.67929356397152,332.916814840802));
#18694=CARTESIAN_POINT('Ctrl Pts',(42.2373353709327,5.36634384842577,339.489429431639));
#18695=CARTESIAN_POINT('Ctrl Pts',(42.5155734052068,-0.871220409715002,
341.942160896935));
#18696=CARTESIAN_POINT('Ctrl Pts',(42.742562154994,-5.30763049058483,338.745836565463));
#18697=CARTESIAN_POINT('Ctrl Pts',(42.8768048933565,-5.90967030800872,335.886470939726));
#18698=CARTESIAN_POINT('Ctrl Pts',(42.9183016202944,-5.90741276477635,335.001689847821));
#18699=CARTESIAN_POINT('',(44.6683016202944,-5.91495147643108,334.99459846622));
#18700=CARTESIAN_POINT('Ctrl Pts',(42.9183016202944,-5.90741276477635,335.001689847821));
#18701=CARTESIAN_POINT('Ctrl Pts',(42.9695509047812,-5.90462465390847,333.908967572269));
#18702=CARTESIAN_POINT('Ctrl Pts',(43.1135462006923,-5.08956830760904,330.834875226341));
#18703=CARTESIAN_POINT('Ctrl Pts',(43.3502875080286,-0.138508694537335,
328.004756025501));
#18704=CARTESIAN_POINT('Ctrl Pts',(43.6285255423024,5.80749489289954,331.097997182194));
#18705=CARTESIAN_POINT('Ctrl Pts',(43.9067635765764,6.42404613560693,337.772048731321));
#18706=CARTESIAN_POINT('Ctrl Pts',(44.1850016108504,1.14534505843243,341.902232075086));
#18707=CARTESIAN_POINT('Ctrl Pts',(44.4388476254232,-4.62951679538216,339.891545450806));
#18708=CARTESIAN_POINT('Ctrl Pts',(44.5999476285711,-5.90200285453643,336.447349225365));
#18709=CARTESIAN_POINT('Ctrl Pts',(44.6683016202944,-5.91495147643108,334.99459846622));
#18710=CARTESIAN_POINT('',(46.4183016202944,-5.92630438040088,335.000973658267));
#18711=CARTESIAN_POINT('Ctrl Pts',(44.6683016202944,-5.91495147643108,334.99459846622));
#18712=CARTESIAN_POINT('Ctrl Pts',(44.6926936399957,-5.91957217278538,334.476186530872));
#18713=CARTESIAN_POINT('Ctrl Pts',(44.8098316711211,-5.61950938738174,331.991874660925));
#18714=CARTESIAN_POINT('Ctrl Pts',(45.0197157136725,-2.12826100431989,328.334932257004));
#18715=CARTESIAN_POINT('Ctrl Pts',(45.297953747946,4.45307350904086,329.60344931977));
#18716=CARTESIAN_POINT('Ctrl Pts',(45.5761917822201,6.94788819041166,335.824301288824));
#18717=CARTESIAN_POINT('Ctrl Pts',(45.8544298164939,3.06672843010346,341.288704131791));
#18718=CARTESIAN_POINT('Ctrl Pts',(46.132667850768,-3.62872274567329,340.982056014135));
#18719=CARTESIAN_POINT('Ctrl Pts',(46.3206251187015,-5.90215834541804,337.066504608215));
#18720=CARTESIAN_POINT('Ctrl Pts',(46.4158363752102,-5.92642313844046,335.05310819842));
#18721=CARTESIAN_POINT('Ctrl Pts',(46.4183016202944,-5.92630438040088,335.000973658267));
#18722=CARTESIAN_POINT('',(48.1683016202945,-5.91203636053623,335.004879585725));
#18723=CARTESIAN_POINT('Ctrl Pts',(46.4183016202944,-5.92630438040088,335.000973658267));
#18724=CARTESIAN_POINT('Ctrl Pts',(46.5085823866349,-5.92195529280249,333.091732963305));
#18725=CARTESIAN_POINT('Ctrl Pts',(46.6916091644001,-3.88205234854485,329.213136309643));
#18726=CARTESIAN_POINT('Ctrl Pts',(46.9673819535897,2.72858646747409,328.557373298822));
#18727=CARTESIAN_POINT('Ctrl Pts',(47.2456199878637,6.89433694424205,333.808051586487));
#18728=CARTESIAN_POINT('Ctrl Pts',(47.5238580221377,4.73325616752653,340.152563340105));
#18729=CARTESIAN_POINT('Ctrl Pts',(47.8020960564115,-1.77146393138185,341.768643768218));
#18730=CARTESIAN_POINT('Ctrl Pts',(48.0169105891306,-5.53836790729106,338.220747892415));
#18731=CARTESIAN_POINT('Ctrl Pts',(48.1389791104248,-5.91687241535322,335.628859529147));
#18732=CARTESIAN_POINT('Ctrl Pts',(48.1683016202945,-5.91203636053623,335.004879585725));
#18733=CARTESIAN_POINT('',(49.9183016202945,-5.90873410525529,334.99676686743));
#18734=CARTESIAN_POINT('Ctrl Pts',(48.1683016202945,-5.91203636053623,335.004879585725));
#18735=CARTESIAN_POINT('Ctrl Pts',(48.2317251218495,-5.90157615329038,333.655234105586));
#18736=CARTESIAN_POINT('Ctrl Pts',(48.3878946348288,-4.77270907439321,330.316143069235));
#18737=CARTESIAN_POINT('Ctrl Pts',(48.6368101592334,0.77734454668611,328.046701618874));
#18738=CARTESIAN_POINT('Ctrl Pts',(48.9150481935072,6.26784268903641,331.890856879023));
#18739=CARTESIAN_POINT('Ctrl Pts',(49.1932862277813,6.00643410886364,338.588226890415));
#18740=CARTESIAN_POINT('Ctrl Pts',(49.4715242620551,0.233009601809311,341.992734046616));
#18741=CARTESIAN_POINT('Ctrl Pts',(49.7131960595596,-4.9673952784858,339.376033223979));
#18742=CARTESIAN_POINT('Ctrl Pts',(49.8621218456393,-5.90281046865438,336.193946273827));
#18743=CARTESIAN_POINT('Ctrl Pts',(49.9183016202945,-5.90873410525529,334.99676686743));
#18744=CARTESIAN_POINT('',(51.6683016202944,-5.92387939532596,334.996491143367));
#18745=CARTESIAN_POINT('Ctrl Pts',(49.9183016202945,-5.90873410525529,334.99676686743));
#18746=CARTESIAN_POINT('Ctrl Pts',(49.954867857064,-5.91258967605129,334.217547906538));
#18747=CARTESIAN_POINT('Ctrl Pts',(50.084180105258,-5.40644147763003,331.466739609232));
#18748=CARTESIAN_POINT('Ctrl Pts',(50.306238364877,-1.23849736786919,328.113872845278));
#18749=CARTESIAN_POINT('Ctrl Pts',(50.5844763991509,5.12046924276799,330.232042611864));
#18750=CARTESIAN_POINT('Ctrl Pts',(50.8627144334248,6.78045680731883,336.725696498605));
#18751=CARTESIAN_POINT('Ctrl Pts',(51.140952467699,2.21811923917046,341.635704179819));
#18752=CARTESIAN_POINT('Ctrl Pts',(51.4094815299885,-4.14952426205602,340.497381424821));
#18753=CARTESIAN_POINT('Ctrl Pts',(51.5852645808539,-5.91154402679634,336.754449414842));
#18754=CARTESIAN_POINT('Ctrl Pts',(51.6683016202944,-5.92387939532596,334.996491143367));
#18755=CARTESIAN_POINT('',(53.4183016202944,-5.91960720730597,335.0051128859));
#18756=CARTESIAN_POINT('Ctrl Pts',(51.6683016202944,-5.92387939532596,334.996491143367));
#18757=CARTESIAN_POINT('Ctrl Pts',(51.6780105922785,-5.92532168840715,334.790944706235));
#18758=CARTESIAN_POINT('Ctrl Pts',(51.7804655756869,-5.82224188165806,332.623356646663));
#18759=CARTESIAN_POINT('Ctrl Pts',(51.9756665705209,-3.1514159100441,328.753304819087));
#18760=CARTESIAN_POINT('Ctrl Pts',(52.2539046047944,3.54756726788876,328.969461931057));
#18761=CARTESIAN_POINT('Ctrl Pts',(52.5321426390685,6.99100032608663,334.719754818285));
#18762=CARTESIAN_POINT('Ctrl Pts',(52.8103806733425,4.01889557202994,340.727224572371));
#18763=CARTESIAN_POINT('Ctrl Pts',(53.0886187076162,-2.6412903296749,341.47890487008));
#18764=CARTESIAN_POINT('Ctrl Pts',(53.2912590232671,-5.72659013567874,337.696184823853));
#18765=CARTESIAN_POINT('Ctrl Pts',(53.4011533274931,-5.92292514524674,335.368837807842));
#18766=CARTESIAN_POINT('Ctrl Pts',(53.4183016202944,-5.91960720730597,335.0051128859));
#18767=CARTESIAN_POINT('',(55.1683016202944,-5.90707311933271,335.000830582995));
#18768=CARTESIAN_POINT('Ctrl Pts',(53.4183016202944,-5.91960720730597,335.0051128859));
#18769=CARTESIAN_POINT('Ctrl Pts',(53.4938993389177,-5.90498018047825,333.401642813176));
#18770=CARTESIAN_POINT('Ctrl Pts',(53.6622430689657,-4.40292613845449,329.806849236265));
#18771=CARTESIAN_POINT('Ctrl Pts',(53.9233328104383,1.67985030475698,328.208039614749));
#18772=CARTESIAN_POINT('Ctrl Pts',(54.201570844712,6.62056777777224,332.73710247224));
#18773=CARTESIAN_POINT('Ctrl Pts',(54.4798088789863,5.48568792054639,339.342792990646));
#18774=CARTESIAN_POINT('Ctrl Pts',(54.7580469132599,-0.683326772745727,
341.963166481054));
#18775=CARTESIAN_POINT('Ctrl Pts',(54.9875444936961,-5.25445185386925,338.853889772642));
#18776=CARTESIAN_POINT('Ctrl Pts',(55.1242960627076,-5.90824604487542,335.939238808905));
#18777=CARTESIAN_POINT('Ctrl Pts',(55.1683016202944,-5.90707311933271,335.000830582995));
#18778=CARTESIAN_POINT('',(56.9183016202944,-5.91655016123008,334.994551668503));
#18779=CARTESIAN_POINT('Ctrl Pts',(55.1683016202944,-5.90707311933271,335.000830582995));
#18780=CARTESIAN_POINT('Ctrl Pts',(55.2170420741322,-5.90577398971354,333.961451801674));
#18781=CARTESIAN_POINT('Ctrl Pts',(55.3585285393945,-5.14861220680334,330.942516361876));
#18782=CARTESIAN_POINT('Ctrl Pts',(55.592761016082,-0.32746797118099,328.01105246485));
#18783=CARTESIAN_POINT('Ctrl Pts',(55.8709990503557,5.69994337564951,330.942504659818));
#18784=CARTESIAN_POINT('Ctrl Pts',(56.1492370846297,6.49660081767273,337.597460439936));
#18785=CARTESIAN_POINT('Ctrl Pts',(56.4274751189038,1.33142357898633,341.868765112781));
#18786=CARTESIAN_POINT('Ctrl Pts',(56.6838299641251,-4.55324881616425,339.996525222044));
#18787=CARTESIAN_POINT('Ctrl Pts',(56.8474387979221,-5.90269240546529,336.499586459046));
#18788=CARTESIAN_POINT('Ctrl Pts',(56.9183016202944,-5.91655016123008,334.994551668503));
#18789=CARTESIAN_POINT('',(58.6683016202944,-5.92574144593171,335.001926606557));
#18790=CARTESIAN_POINT('Ctrl Pts',(56.9183016202944,-5.91655016123008,334.994551668503));
#18791=CARTESIAN_POINT('Ctrl Pts',(56.9401848093468,-5.92082958278134,334.529781006691));
#18792=CARTESIAN_POINT('Ctrl Pts',(57.0548140098239,-5.65820055662157,332.099986169156));
#18793=CARTESIAN_POINT('Ctrl Pts',(57.2621892217253,-2.30757253733108,328.394870788079));
#18794=CARTESIAN_POINT('Ctrl Pts',(57.5404272559994,4.30563416012261,329.485098604652));
#18795=CARTESIAN_POINT('Ctrl Pts',(57.8186652902734,6.96762393988721,335.636270031926));
#18796=CARTESIAN_POINT('Ctrl Pts',(58.0969033245473,3.23552807197775,341.203545842231));
#18797=CARTESIAN_POINT('Ctrl Pts',(58.3751413588211,-3.4657641512668,341.077919197307));
#18798=CARTESIAN_POINT('Ctrl Pts',(58.5656074574036,-5.8759136268268,337.173799765407));
#18799=CARTESIAN_POINT('Ctrl Pts',(58.6633275445613,-5.92618778307363,335.107144141683));
#18800=CARTESIAN_POINT('Ctrl Pts',(58.6683016202944,-5.92574144593171,335.001926606557));
#18801=CARTESIAN_POINT('',(60.4183016202944,-5.91073449090133,335.004414681335));
#18802=CARTESIAN_POINT('Ctrl Pts',(58.6683016202944,-5.92574144593171,335.001926606557));
#18803=CARTESIAN_POINT('Ctrl Pts',(58.7560735559859,-5.91786543498634,333.145270772946));
#18804=CARTESIAN_POINT('Ctrl Pts',(58.9365915031022,-3.9770378638174,329.312552672385));
#18805=CARTESIAN_POINT('Ctrl Pts',(59.209855461643,2.55351200167337,328.485999740673));
#18806=CARTESIAN_POINT('Ctrl Pts',(59.4880934959169,6.85961365276339,333.622203405417));
#18807=CARTESIAN_POINT('Ctrl Pts',(59.7663315301909,4.87074910244332,340.022790668771));
#18808=CARTESIAN_POINT('Ctrl Pts',(60.0445695644648,-1.58793000704763,341.814037071656));
#18809=CARTESIAN_POINT('Ctrl Pts',(60.2618929278326,-5.49441940395862,338.328985156489));
#18810=CARTESIAN_POINT('Ctrl Pts',(60.3864702797759,-5.9154146125806,335.682158166079));
#18811=CARTESIAN_POINT('Ctrl Pts',(60.4183016202944,-5.91073449090133,335.004414681335));
#18812=CARTESIAN_POINT('',(62.1683016202944,-5.90971298490255,334.996095888348));
#18813=CARTESIAN_POINT('Ctrl Pts',(60.4183016202944,-5.91073449090133,335.004414681335));
#18814=CARTESIAN_POINT('Ctrl Pts',(60.4792162912005,-5.90177828399176,333.707437530533));
#18815=CARTESIAN_POINT('Ctrl Pts',(60.6328769735312,-4.84222249885208,330.422433708709));
#18816=CARTESIAN_POINT('Ctrl Pts',(60.8792836672866,0.589184251637315,328.028236604786));
#18817=CARTESIAN_POINT('Ctrl Pts',(61.1575217015605,6.18154598103065,331.722636394047));
#18818=CARTESIAN_POINT('Ctrl Pts',(61.4357597358347,6.10119420310092,338.424624390686));
#18819=CARTESIAN_POINT('Ctrl Pts',(61.7139977701083,0.421866558465273,341.98388513136));
#18820=CARTESIAN_POINT('Ctrl Pts',(61.9581783982619,-4.90204272784256,339.482957637104));
#18821=CARTESIAN_POINT('Ctrl Pts',(62.1096130149904,-5.90216516025079,336.246218920781));
#18822=CARTESIAN_POINT('Ctrl Pts',(62.1683016202944,-5.90971298490255,334.996095888348));
#18823=CARTESIAN_POINT('',(63.9183016202944,-5.92498055086206,334.99728658688));
#18824=CARTESIAN_POINT('Ctrl Pts',(62.1683016202944,-5.90971298490255,334.996095888348));
#18825=CARTESIAN_POINT('Ctrl Pts',(62.202359026415,-5.91409304007954,334.270640791982));
#18826=CARTESIAN_POINT('Ctrl Pts',(62.3291624439605,-5.45388643310246,331.574970920775));
#18827=CARTESIAN_POINT('Ctrl Pts',(62.5487118729301,-1.42410672731237,328.149850881153));
#18828=CARTESIAN_POINT('Ctrl Pts',(62.8269499072042,4.98977067018535,330.095429521337));
#18829=CARTESIAN_POINT('Ctrl Pts',(63.1051879414782,6.82460917254905,336.541860098449));
#18830=CARTESIAN_POINT('Ctrl Pts',(63.3834259757519,2.39660456833038,341.57334842103));
#18831=CARTESIAN_POINT('Ctrl Pts',(63.6544638686909,-4.0592289865778,340.598469645657));
#18832=CARTESIAN_POINT('Ctrl Pts',(63.8327557502049,-5.91467205800235,336.807471137171));
#18833=CARTESIAN_POINT('Ctrl Pts',(63.9183016202944,-5.92498055086206,334.99728658688));
#18834=CARTESIAN_POINT('',(65.6683016202944,-5.91799273079897,335.005359985955));
#18835=CARTESIAN_POINT('Ctrl Pts',(63.9183016202944,-5.92498055086206,334.99728658688));
#18836=CARTESIAN_POINT('Ctrl Pts',(63.9255017616296,-5.92584818603211,334.844928739666));
#18837=CARTESIAN_POINT('Ctrl Pts',(63.9327019029648,-5.92048219266218,334.692632997525));
#18838=CARTESIAN_POINT('Ctrl Pts',(64.0326480557246,-5.756739625575,332.585530948395));
#18839=CARTESIAN_POINT('Ctrl Pts',(64.2181400785738,-3.31904956051073,328.840736006949));
#18840=CARTESIAN_POINT('Ctrl Pts',(64.4963781128479,3.38332832967515,328.875809250616));
#18841=CARTESIAN_POINT('Ctrl Pts',(64.7746161471218,6.98087574956347,334.530961952088));
#18842=CARTESIAN_POINT('Ctrl Pts',(65.0528541813957,4.17217653163317,340.616543947135));
#18843=CARTESIAN_POINT('Ctrl Pts',(65.3310922156696,-2.46526750815017,341.547906461952));
#18844=CARTESIAN_POINT('Ctrl Pts',(65.5362413619692,-5.69109873615545,337.804148014749));
#18845=CARTESIAN_POINT('Ctrl Pts',(65.6486444968441,-5.92186363827105,335.422591367118));
#18846=CARTESIAN_POINT('Ctrl Pts',(65.6683016202944,-5.91799273079897,335.005359985955));
#18847=CARTESIAN_POINT('',(67.4183016202943,-5.90696810045156,334.999950211039));
#18848=CARTESIAN_POINT('Ctrl Pts',(65.6683016202944,-5.91799273079897,335.005359985955));
#18849=CARTESIAN_POINT('Ctrl Pts',(65.7413905082688,-5.90359996762069,333.454015113223));
#18850=CARTESIAN_POINT('Ctrl Pts',(65.9072254076679,-4.48362293751429,329.91077451435));
#18851=CARTESIAN_POINT('Ctrl Pts',(66.1658063184914,1.49571981909767,328.165130202852));
#18852=CARTESIAN_POINT('Ctrl Pts',(66.4440443527656,6.55700764647546,332.559042473679));
#18853=CARTESIAN_POINT('Ctrl Pts',(66.7222823870391,5.60102633795406,339.192985437936));
#18854=CARTESIAN_POINT('Ctrl Pts',(67.0005204213133,-0.494934169890714,
341.979087554164));
#18855=CARTESIAN_POINT('Ctrl Pts',(67.2325268323983,-5.19927322096242,338.961829264472));
#18856=CARTESIAN_POINT('Ctrl Pts',(67.3717872320586,-5.90689385452013,335.991902632384));
#18857=CARTESIAN_POINT('Ctrl Pts',(67.4183016202943,-5.90696810045156,334.999950211039));
#18858=CARTESIAN_POINT('',(69.1683016202943,-5.91817602837582,334.994660059035));
#18859=CARTESIAN_POINT('Ctrl Pts',(67.4183016202943,-5.90696810045156,334.999950211039));
#18860=CARTESIAN_POINT('Ctrl Pts',(67.4645332434833,-5.90704189503546,334.014027955488));
#18861=CARTESIAN_POINT('Ctrl Pts',(67.6035108780967,-5.20559334401723,331.050329750945));
#18862=CARTESIAN_POINT('Ctrl Pts',(67.8352345241351,-0.516188130390139,
328.022452240558));
#18863=CARTESIAN_POINT('Ctrl Pts',(68.1134725584092,5.58822975414558,330.789974924528));
#18864=CARTESIAN_POINT('Ctrl Pts',(68.3917105926828,6.56441167543405,337.420975480384));
#18865=CARTESIAN_POINT('Ctrl Pts',(68.6699486269569,1.51652989273906,341.830282571435));
#18866=CARTESIAN_POINT('Ctrl Pts',(68.9288123028274,-4.4746462044703,340.100968698183));
#18867=CARTESIAN_POINT('Ctrl Pts',(69.0949299672732,-5.90373615388174,336.551882931456));
#18868=CARTESIAN_POINT('Ctrl Pts',(69.1683016202943,-5.91817602837582,334.994660059035));
#18869=CARTESIAN_POINT('',(70.9183016202944,-5.92486842591992,335.002808317045));
#18870=CARTESIAN_POINT('Ctrl Pts',(69.1683016202943,-5.91817602837582,334.994660059035));
#18871=CARTESIAN_POINT('Ctrl Pts',(69.1876759786978,-5.92198899008828,334.58346318937));
#18872=CARTESIAN_POINT('Ctrl Pts',(69.2997963485261,-5.69518240152726,332.20802472484));
#18873=CARTESIAN_POINT('Ctrl Pts',(69.5046627297787,-2.48519907860735,328.459632390995));
#18874=CARTESIAN_POINT('Ctrl Pts',(69.7829007640527,4.15505083290677,329.370774875957));
#18875=CARTESIAN_POINT('Ctrl Pts',(70.0611387983268,6.98227192351401,335.447774170024));
#18876=CARTESIAN_POINT('Ctrl Pts',(70.3393768326004,3.4019651280758,341.113857717396));
#18877=CARTESIAN_POINT('Ctrl Pts',(70.6176148668744,-3.300274852473,341.169344277907));
#18878=CARTESIAN_POINT('Ctrl Pts',(70.8105897961057,-5.84815730883804,337.281223184853));
#18879=CARTESIAN_POINT('Ctrl Pts',(70.9108187139124,-5.92579638347857,335.161157513766));
#18880=CARTESIAN_POINT('Ctrl Pts',(70.9183016202944,-5.92486842591992,335.002808317045));
#18881=CARTESIAN_POINT('',(72.6683004134488,-5.91269508019852,335.00386097788));
#18882=CARTESIAN_POINT('Ctrl Pts',(70.9183016202944,-5.92486842591992,335.002808317045));
#18883=CARTESIAN_POINT('Ctrl Pts',(71.003564725337,-5.914294921621,333.198516842018));
#18884=CARTESIAN_POINT('Ctrl Pts',(71.1815738418041,-4.06952942461849,329.412881975299));
#18885=CARTESIAN_POINT('Ctrl Pts',(71.4523289696966,2.37657295890068,328.419382711913));
#18886=CARTESIAN_POINT('Ctrl Pts',(71.7305670039699,6.81988146465013,333.437361292776));
#18887=CARTESIAN_POINT('Ctrl Pts',(72.0088050382442,5.00468541158024,339.889350350746));
#18888=CARTESIAN_POINT('Ctrl Pts',(72.287043072518,-1.40323657466442,341.854454758531));
#18889=CARTESIAN_POINT('Ctrl Pts',(72.5068745564487,-5.44861993418268,338.437239673097));
#18890=CARTESIAN_POINT('Ctrl Pts',(72.6339600289546,-5.91391880206817,335.735378916058));
#18891=CARTESIAN_POINT('Ctrl Pts',(72.6682994900359,-5.90959342734641,335.003878636489));
#18892=CARTESIAN_POINT('',(74.4183028417416,-5.91333520907357,334.995498940171));
#18893=CARTESIAN_POINT('Ctrl Pts',(72.6683016202943,-5.91674875527348,335.003837899133));
#18894=CARTESIAN_POINT('Ctrl Pts',(72.6757466628066,-5.91685175174843,334.845051999899));
#18895=CARTESIAN_POINT('Ctrl Pts',(72.6831917053189,-5.91055848980237,334.686234110631));
#18896=CARTESIAN_POINT('Ctrl Pts',(72.6906367478312,-5.89788795012559,334.52793190082));
#18897=CARTESIAN_POINT('Ctrl Pts',(72.6980821561644,-5.88521678786688,334.369621912643));
#18898=CARTESIAN_POINT('Ctrl Pts',(72.7055275644977,-5.866167751949,334.211828019704));
#18899=CARTESIAN_POINT('Ctrl Pts',(72.7129729728309,-5.84081179818755,334.055093602174));
#18900=CARTESIAN_POINT('Ctrl Pts',(72.7204201449255,-5.81544983779108,333.898322055437));
#18901=CARTESIAN_POINT('Ctrl Pts',(72.7278673170201,-5.7837780416924,333.742610845743));
#18902=CARTESIAN_POINT('Ctrl Pts',(72.7353144891147,-5.74591865285806,333.588493925894));
#18903=CARTESIAN_POINT('Ctrl Pts',(72.7427648236843,-5.70804318686424,333.434311559603));
#18904=CARTESIAN_POINT('Ctrl Pts',(72.7502151582539,-5.66397498144229,333.28172518725));
#18905=CARTESIAN_POINT('Ctrl Pts',(72.7576654928236,-5.61388635854149,333.131254293414));
#18906=CARTESIAN_POINT('Ctrl Pts',(72.7651251739802,-5.563734898507,332.98059463097));
#18907=CARTESIAN_POINT('Ctrl Pts',(72.7725848551368,-5.50754804852549,332.83205609678));
#18908=CARTESIAN_POINT('Ctrl Pts',(72.7800445362934,-5.44554693405786,332.686139772702));
#18909=CARTESIAN_POINT('Ctrl Pts',(72.787509142231,-5.38350488728905,332.540127116631));
#18910=CARTESIAN_POINT('Ctrl Pts',(72.7949737481687,-5.31564108124781,332.396740451863));
#18911=CARTESIAN_POINT('Ctrl Pts',(72.8024383541064,-5.24222280121369,332.256456549472));
#18912=CARTESIAN_POINT('Ctrl Pts',(72.8099152313152,-5.16868382684847,332.115942030513));
#18913=CARTESIAN_POINT('Ctrl Pts',(72.8173921085241,-5.08957231441577,331.978540783871));
#18914=CARTESIAN_POINT('Ctrl Pts',(72.8248689857329,-5.00519974560868,331.844701904881));
#18915=CARTESIAN_POINT('Ctrl Pts',(72.8310857041772,-4.93504739589738,331.733420335805));
#18916=CARTESIAN_POINT('Ctrl Pts',(72.8373024226216,-4.86125878684599,331.624601054125));
#18917=CARTESIAN_POINT('Ctrl Pts',(72.843519141066,-4.78403375003706,331.518484289709));
#18918=CARTESIAN_POINT('Ctrl Pts',(72.850943118504,-4.69181195552443,331.391760122952));
#18919=CARTESIAN_POINT('Ctrl Pts',(72.858367095942,-4.59441237210414,331.268511608734));
#18920=CARTESIAN_POINT('Ctrl Pts',(72.86579107338,-4.4921259084281,331.149190294843));
#18921=CARTESIAN_POINT('Ctrl Pts',(72.8732062894076,-4.38996015816917,331.030009798056));
#18922=CARTESIAN_POINT('Ctrl Pts',(72.8806215054352,-4.28291924800103,330.914747556773));
#18923=CARTESIAN_POINT('Ctrl Pts',(72.8880367214629,-4.17133698706704,330.803825753996));
#18924=CARTESIAN_POINT('Ctrl Pts',(72.895444802607,-4.05986209002254,330.693010679619));
#18925=CARTESIAN_POINT('Ctrl Pts',(72.9028528837511,-3.94385480431372,330.586527990774));
#18926=CARTESIAN_POINT('Ctrl Pts',(72.9102609648952,-3.82368870328334,330.484766311376));
#18927=CARTESIAN_POINT('Ctrl Pts',(72.9176635320692,-3.70361204407653,330.383080375055));
#18928=CARTESIAN_POINT('Ctrl Pts',(72.9250660992432,-3.57938301669183,330.286108691581));
#18929=CARTESIAN_POINT('Ctrl Pts',(72.9324686664172,-3.45141140822068,330.194202474749));
#18930=CARTESIAN_POINT('Ctrl Pts',(72.939867336172,-3.3235071762419,330.102344646139));
#18931=CARTESIAN_POINT('Ctrl Pts',(72.9472660059268,-3.19186458982209,330.015547189946));
#18932=CARTESIAN_POINT('Ctrl Pts',(72.9546646756815,-3.05692572296192,329.934120442925));
#18933=CARTESIAN_POINT('Ctrl Pts',(72.9620621248855,-2.9220091168248,329.852707128789));
#18934=CARTESIAN_POINT('Ctrl Pts',(72.9694595740896,-2.78379762871289,329.776662958035));
#18935=CARTESIAN_POINT('Ctrl Pts',(72.9768570232935,-2.64276156269015,329.706254455939));
#18936=CARTESIAN_POINT('Ctrl Pts',(72.984254151757,-2.50173161174534,329.635849006632));
#18937=CARTESIAN_POINT('Ctrl Pts',(72.9916512802205,-2.35787766031198,329.571078906826));
#18938=CARTESIAN_POINT('Ctrl Pts',(72.999048408684,-2.21169357076184,329.512164168677));
#18939=CARTESIAN_POINT('Ctrl Pts',(73.0064466761206,-2.06548697251136,329.453240359129));
#18940=CARTESIAN_POINT('Ctrl Pts',(73.0138449435572,-1.91694986793742,329.400173845919));
#18941=CARTESIAN_POINT('Ctrl Pts',(73.0212432109939,-1.76659485640011,329.353135987485));
#18942=CARTESIAN_POINT('Ctrl Pts',(73.0286440775196,-1.61618702356597,329.306081604156));
#18943=CARTESIAN_POINT('Ctrl Pts',(73.0360449440454,-1.463960368181,329.265060203762));
#18944=CARTESIAN_POINT('Ctrl Pts',(73.0434458105711,-1.3104412093603,329.230192862902));
#18945=CARTESIAN_POINT('Ctrl Pts',(73.0508548039559,-1.15675347182609,329.195287234368));
#18946=CARTESIAN_POINT('Ctrl Pts',(73.0582637973407,-1.00177076061318,329.166549243657));
#18947=CARTESIAN_POINT('Ctrl Pts',(73.0656727907254,-0.846028839445353,
329.144048688272));
#18948=CARTESIAN_POINT('Ctrl Pts',(73.0730863483057,-0.690190975881867,
329.121534271769));
#18949=CARTESIAN_POINT('Ctrl Pts',(73.0804999058859,-0.533593340756334,
329.10526498571));
#18950=CARTESIAN_POINT('Ctrl Pts',(73.0879134634662,-0.376774811138188,
329.095258574316));
#18951=CARTESIAN_POINT('Ctrl Pts',(73.0953375756029,-0.219733021633884,
329.085237916963));
#18952=CARTESIAN_POINT('Ctrl Pts',(73.1027616877396,-0.0624700816495047,
329.081497950858));
#18953=CARTESIAN_POINT('Ctrl Pts',(73.1101857998763,0.094476318035277,329.084004328278));
#18954=CARTESIAN_POINT('Ctrl Pts',(73.1140429250308,0.176016291434689,329.085306492257));
#18955=CARTESIAN_POINT('Ctrl Pts',(73.1179000501854,0.257470915657662,329.088293828118));
#18956=CARTESIAN_POINT('Ctrl Pts',(73.12175717534,0.338765665720255,329.092956036542));
#18957=CARTESIAN_POINT('Ctrl Pts',(73.1291811527779,0.495237225783612,329.10192959295));
#18958=CARTESIAN_POINT('Ctrl Pts',(73.136605130216,0.651588034156824,329.117138137535));
#18959=CARTESIAN_POINT('Ctrl Pts',(73.1440291076539,0.807280947306682,329.138581397425));
#18960=CARTESIAN_POINT('Ctrl Pts',(73.1514443236816,0.962790119393649,329.159999351041));
#18961=CARTESIAN_POINT('Ctrl Pts',(73.1588595397092,1.11764257559865,329.187637323515));
#18962=CARTESIAN_POINT('Ctrl Pts',(73.1662747557368,1.27130264994705,329.221443075063));
#18963=CARTESIAN_POINT('Ctrl Pts',(73.1736828368809,1.42481487334559,329.255216298887));
#18964=CARTESIAN_POINT('Ctrl Pts',(73.181090918025,1.57713663689715,329.295145407437));
#18965=CARTESIAN_POINT('Ctrl Pts',(73.1884989991691,1.72773897648957,329.341126561619));
#18966=CARTESIAN_POINT('Ctrl Pts',(73.1959015663431,1.8782292200102,329.387073491187));
#18967=CARTESIAN_POINT('Ctrl Pts',(73.2033041335171,2.02700223242095,329.439063388463));
#18968=CARTESIAN_POINT('Ctrl Pts',(73.2107067006911,2.17354091124083,329.496941716676));
#18969=CARTESIAN_POINT('Ctrl Pts',(73.2181053704458,2.32000243808726,329.554789572202));
#18970=CARTESIAN_POINT('Ctrl Pts',(73.2255040402006,2.46423162790464,329.61851954761));
#18971=CARTESIAN_POINT('Ctrl Pts',(73.2329027099554,2.60572828028658,329.687927834468));
#18972=CARTESIAN_POINT('Ctrl Pts',(73.2403001591593,2.74720159011418,329.757324671115));
#18973=CARTESIAN_POINT('Ctrl Pts',(73.2476976083633,2.88594292242243,329.832397795872));
#18974=CARTESIAN_POINT('Ctrl Pts',(73.2550950575673,3.02147364190742,329.912895952139));
#18975=CARTESIAN_POINT('Ctrl Pts',(73.2624921860308,3.15699848501659,329.993390618147));
#18976=CARTESIAN_POINT('Ctrl Pts',(73.2698893144942,3.28931267121137,330.079309657384));
#18977=CARTESIAN_POINT('Ctrl Pts',(73.2772864429577,3.41796393030806,330.170356831648));
#18978=CARTESIAN_POINT('Ctrl Pts',(73.2846847103943,3.54663499848744,330.261418024904));
#18979=CARTESIAN_POINT('Ctrl Pts',(73.2920829778309,3.67164171191348,330.357608709786));
#18980=CARTESIAN_POINT('Ctrl Pts',(73.2994812452675,3.79256257469101,330.458590562441));
#18981=CARTESIAN_POINT('Ctrl Pts',(73.3068821117933,3.91352591823918,330.559607891082));
#18982=CARTESIAN_POINT('Ctrl Pts',(73.3142829783191,4.03040026697695,330.665419499647));
#18983=CARTESIAN_POINT('Ctrl Pts',(73.3216838448448,4.14279898353354,330.77564831666));
#18984=CARTESIAN_POINT('Ctrl Pts',(73.3290928382296,4.25532112462658,330.885998175453));
#18985=CARTESIAN_POINT('Ctrl Pts',(73.3365018316143,4.36335755205725,331.000774667963));
#18986=CARTESIAN_POINT('Ctrl Pts',(73.3439108249991,4.4665596391218,331.119565030481));
#18987=CARTESIAN_POINT('Ctrl Pts',(73.3513243825793,4.56982530223201,331.23842857196));
#18988=CARTESIAN_POINT('Ctrl Pts',(73.3587379401596,4.6682504579066,331.361310619982));
#18989=CARTESIAN_POINT('Ctrl Pts',(73.3661514977398,4.76152856734693,331.487767623741));
#18990=CARTESIAN_POINT('Ctrl Pts',(73.3735756098765,4.85493947525257,331.614404662196));
#18991=CARTESIAN_POINT('Ctrl Pts',(73.3809997220132,4.94318849311046,331.744626513227));
#18992=CARTESIAN_POINT('Ctrl Pts',(73.3884238341499,5.02601352931828,331.877962433665));
#18993=CARTESIAN_POINT('Ctrl Pts',(73.3922809593045,5.06904447021877,331.947235812524));
#18994=CARTESIAN_POINT('Ctrl Pts',(73.3961380844592,5.11061212679421,332.017349362641));
#18995=CARTESIAN_POINT('Ctrl Pts',(73.3999952096138,5.15068483021869,332.088234840813));
#18996=CARTESIAN_POINT('Ctrl Pts',(73.4074191870518,5.22781451467929,332.22467122012));
#18997=CARTESIAN_POINT('Ctrl Pts',(73.4148431644898,5.29963571889571,332.36438016662));
#18998=CARTESIAN_POINT('Ctrl Pts',(73.4222671419278,5.36585799314562,332.506909837191));
#18999=CARTESIAN_POINT('Ctrl Pts',(73.4296823579555,5.43200211514819,332.649271301306));
#19000=CARTESIAN_POINT('Ctrl Pts',(73.4370975739831,5.49256030394941,332.794446528133));
#19001=CARTESIAN_POINT('Ctrl Pts',(73.4445127900107,5.54728660950183,332.941956794783));
#19002=CARTESIAN_POINT('Ctrl Pts',(73.4519208711548,5.60196025767868,333.089325127797));
#19003=CARTESIAN_POINT('Ctrl Pts',(73.4593289522989,5.65081306492765,333.239023680178));
#19004=CARTESIAN_POINT('Ctrl Pts',(73.466737033443,5.69364609892541,333.390551441427));
#19005=CARTESIAN_POINT('Ctrl Pts',(73.474139600617,5.73644725151356,333.541966417796));
#19006=CARTESIAN_POINT('Ctrl Pts',(73.481542167791,5.77323745134734,333.695207534461));
#19007=CARTESIAN_POINT('Ctrl Pts',(73.488944734965,5.80386681787057,333.8497563202));
#19008=CARTESIAN_POINT('Ctrl Pts',(73.4963434047197,5.83448005816613,334.004223736677));
#19009=CARTESIAN_POINT('Ctrl Pts',(73.5037420744744,5.85893885270495,334.159997085907));
#19010=CARTESIAN_POINT('Ctrl Pts',(73.5111407442292,5.87714390120493,334.316545446259));
#19011=CARTESIAN_POINT('Ctrl Pts',(73.5185381934331,5.89534594643729,334.473067980992));
#19012=CARTESIAN_POINT('Ctrl Pts',(73.5259356426371,5.90729625010176,334.630364902748));
#19013=CARTESIAN_POINT('Ctrl Pts',(73.5333330918411,5.91294708220821,334.787897747524));
#19014=CARTESIAN_POINT('Ctrl Pts',(73.5407302203046,5.91859766930443,334.94542376195));
#19015=CARTESIAN_POINT('Ctrl Pts',(73.5481273487681,5.91794931454442,335.103185306085));
#19016=CARTESIAN_POINT('Ctrl Pts',(73.5555244772315,5.91100638160463,335.260641744794));
#19017=CARTESIAN_POINT('Ctrl Pts',(73.5629227446682,5.90406237962649,335.418122427864));
#19018=CARTESIAN_POINT('Ctrl Pts',(73.5703210121048,5.89082188608956,335.575297539095));
#19019=CARTESIAN_POINT('Ctrl Pts',(73.5777192795414,5.87134130912532,335.731629547147));
#19020=CARTESIAN_POINT('Ctrl Pts',(73.5851201460671,5.85185388842959,335.888016476277));
#19021=CARTESIAN_POINT('Ctrl Pts',(73.5925210125928,5.82612206574632,336.043559342399));
#19022=CARTESIAN_POINT('Ctrl Pts',(73.5999218791186,5.79425369685743,336.197728958886));
#19023=CARTESIAN_POINT('Ctrl Pts',(73.6073308725034,5.76235033345261,336.352067868352));
#19024=CARTESIAN_POINT('Ctrl Pts',(73.6147398658881,5.72429704226325,336.505030151006));
#19025=CARTESIAN_POINT('Ctrl Pts',(73.6221488592729,5.68025226318593,336.656099269087));
#19026=CARTESIAN_POINT('Ctrl Pts',(73.6295624168531,5.63618035100563,336.807261450955));
#19027=CARTESIAN_POINT('Ctrl Pts',(73.6369759744334,5.58610971461997,336.956527791325));
#19028=CARTESIAN_POINT('Ctrl Pts',(73.6443895320136,5.53024745963212,337.10340048439));
#19029=CARTESIAN_POINT('Ctrl Pts',(73.6518136441503,5.47430567449726,337.250482277622));
#19030=CARTESIAN_POINT('Ctrl Pts',(73.659237756287,5.41255594909426,337.395163275171));
#19031=CARTESIAN_POINT('Ctrl Pts',(73.6666618684236,5.34525230859312,337.536968332475));
#19032=CARTESIAN_POINT('Ctrl Pts',(73.6705189935784,5.31028535766301,337.610641768911));
#19033=CARTESIAN_POINT('Ctrl Pts',(73.6743761187332,5.27382002168621,337.683539363217));
#19034=CARTESIAN_POINT('Ctrl Pts',(73.6782332438879,5.23589655000898,337.755597554089));
#19035=CARTESIAN_POINT('Ctrl Pts',(73.6856572213259,5.1629035858694,337.894291104803));
#19036=CARTESIAN_POINT('Ctrl Pts',(73.6930811987639,5.08428592689864,338.030291615116));
#19037=CARTESIAN_POINT('Ctrl Pts',(73.7005051762019,5.00026635860841,338.163110321419));
#19038=CARTESIAN_POINT('Ctrl Pts',(73.7079203922295,4.91634594605024,338.295772281666));
#19039=CARTESIAN_POINT('Ctrl Pts',(73.7153356082571,4.82703651142196,338.42525959997));
#19040=CARTESIAN_POINT('Ctrl Pts',(73.7227508242848,4.73260752533167,338.551106387265));
#19041=CARTESIAN_POINT('Ctrl Pts',(73.7301589054289,4.63826939833633,338.676832085415));
#19042=CARTESIAN_POINT('Ctrl Pts',(73.737566986573,4.53882174913629,338.798923929654));
#19043=CARTESIAN_POINT('Ctrl Pts',(73.744975067717,4.43457823445391,338.916943508018));
#19044=CARTESIAN_POINT('Ctrl Pts',(73.7523776348911,4.330412310123,339.034875242256));
#19045=CARTESIAN_POINT('Ctrl Pts',(73.7597802020651,4.22145787401434,339.148740467382));
#19046=CARTESIAN_POINT('Ctrl Pts',(73.7671827692392,4.10806981067076,339.258132571111));
#19047=CARTESIAN_POINT('Ctrl Pts',(73.7745814389939,3.99474144564777,339.367467080375));
#19048=CARTESIAN_POINT('Ctrl Pts',(73.7819801087486,3.87698437017182,339.472332900049));
#19049=CARTESIAN_POINT('Ctrl Pts',(73.7893787785033,3.75519131048829,339.57235921425));
#19050=CARTESIAN_POINT('Ctrl Pts',(73.7967762277073,3.63341834287722,339.672369027215));
#19051=CARTESIAN_POINT('Ctrl Pts',(73.8041736769112,3.50761100061101,339.767540682572));
#19052=CARTESIAN_POINT('Ctrl Pts',(73.8115711261152,3.37819626012077,339.857542649386));
#19053=CARTESIAN_POINT('Ctrl Pts',(73.8189682545787,3.24878713082816,339.947540713872));
#19054=CARTESIAN_POINT('Ctrl Pts',(73.8263653830422,3.11577122070671,340.032369322409));
#19055=CARTESIAN_POINT('Ctrl Pts',(73.8337625115056,2.9796055228116,340.111739575813));
#19056=CARTESIAN_POINT('Ctrl Pts',(73.8411607789423,2.84341885879757,340.191122050254));
#19057=CARTESIAN_POINT('Ctrl Pts',(73.8485590463789,2.70408176378673,340.265044308159));
#19058=CARTESIAN_POINT('Ctrl Pts',(73.8559573138155,2.56207678502752,340.333262895276));
#19059=CARTESIAN_POINT('Ctrl Pts',(73.8633581803413,2.42002191842632,340.401505448299));
#19060=CARTESIAN_POINT('Ctrl Pts',(73.870759046867,2.27529763819714,340.464040179546));
#19061=CARTESIAN_POINT('Ctrl Pts',(73.8781599133928,2.12840731561548,340.520671413998));
#19062=CARTESIAN_POINT('Ctrl Pts',(73.8855689067775,1.98135569341636,340.577364834959));
#19063=CARTESIAN_POINT('Ctrl Pts',(73.8929779001623,1.83213362726564,340.628141678684));
#19064=CARTESIAN_POINT('Ctrl Pts',(73.9003868935471,1.68126122570574,340.672855652442));
#19065=CARTESIAN_POINT('Ctrl Pts',(73.9078004511273,1.53029588154245,340.717597171549));
#19066=CARTESIAN_POINT('Ctrl Pts',(73.9152140087075,1.37767853706626,340.756268286877));
#19067=CARTESIAN_POINT('Ctrl Pts',(73.9226275662878,1.223939884527,340.788773766659));
#19068=CARTESIAN_POINT('Ctrl Pts',(73.9300516784245,1.06998235687021,340.821325523943));
#19069=CARTESIAN_POINT('Ctrl Pts',(73.9374757905612,0.914900699783915,340.847694052046));
#19070=CARTESIAN_POINT('Ctrl Pts',(73.9448999026978,0.75923194006135,340.867835838168));
#19071=CARTESIAN_POINT('Ctrl Pts',(73.9487570278525,0.678355752059643,340.87830030698));
#19072=CARTESIAN_POINT('Ctrl Pts',(73.9526141530071,0.597321124130932,340.887084899145));
#19073=CARTESIAN_POINT('Ctrl Pts',(73.9564712781617,0.516203287562623,340.894189064529));
#19074=CARTESIAN_POINT('Ctrl Pts',(73.9638952555997,0.360072240640283,340.907862762272));
#19075=CARTESIAN_POINT('Ctrl Pts',(73.9713192330376,0.203161983725986,340.915349175448));
#19076=CARTESIAN_POINT('Ctrl Pts',(73.9787432104756,0.0460040905896751,
340.91657115111));
#19077=CARTESIAN_POINT('Ctrl Pts',(73.9861584265032,-0.110968332587724,
340.917791684658));
#19078=CARTESIAN_POINT('Ctrl Pts',(73.9935736425308,-0.268187440692085,
340.912762493661));
#19079=CARTESIAN_POINT('Ctrl Pts',(74.0009888585585,-0.425115631659458,
340.901458062396));
#19080=CARTESIAN_POINT('Ctrl Pts',(74.0083969397025,-0.581892827110618,
340.890164508198));
#19081=CARTESIAN_POINT('Ctrl Pts',(74.0158050208466,-0.738379292932514,
340.87260776091));
#19082=CARTESIAN_POINT('Ctrl Pts',(74.0232131019906,-0.894036621501628,
340.848814331291));
#19083=CARTESIAN_POINT('Ctrl Pts',(74.0306156691646,-1.049578091478,340.825038611556));
#19084=CARTESIAN_POINT('Ctrl Pts',(74.0380182363385,-1.20429128567534,340.795035508693));
#19085=CARTESIAN_POINT('Ctrl Pts',(74.0454208035125,-1.35764222675871,340.758883411445));
#19086=CARTESIAN_POINT('Ctrl Pts',(74.0528194732672,-1.51091242924302,340.722750348119));
#19087=CARTESIAN_POINT('Ctrl Pts',(74.060218143022,-1.66282144466149,340.680474823339));
#19088=CARTESIAN_POINT('Ctrl Pts',(74.0676168127767,-1.81284491932002,340.632186419233));
#19089=CARTESIAN_POINT('Ctrl Pts',(74.0750142619807,-1.96284364476317,340.583905981214));
#19090=CARTESIAN_POINT('Ctrl Pts',(74.0824117111846,-2.11095709187498,340.529614746784));
#19091=CARTESIAN_POINT('Ctrl Pts',(74.0898091603886,-2.25667540777178,340.469492359119));
#19092=CARTESIAN_POINT('Ctrl Pts',(74.097206288852,-2.40238740557655,340.409372578255));
#19093=CARTESIAN_POINT('Ctrl Pts',(74.1046034173155,-2.54570413365216,340.343422289209));
#19094=CARTESIAN_POINT('Ctrl Pts',(74.1120005457789,-2.68613534534628,340.271869447263));
#19095=CARTESIAN_POINT('Ctrl Pts',(74.1193988132155,-2.82658817994117,340.200305587965));
#19096=CARTESIAN_POINT('Ctrl Pts',(74.1267970806521,-2.96415428094545,340.123137627555));
#19097=CARTESIAN_POINT('Ctrl Pts',(74.1341953480886,-3.09836778848121,340.040639603245));
#19098=CARTESIAN_POINT('Ctrl Pts',(74.1415962146144,-3.23262844663473,339.958112596511));
#19099=CARTESIAN_POINT('Ctrl Pts',(74.1489970811402,-3.36353384857073,339.870251993029));
#19100=CARTESIAN_POINT('Ctrl Pts',(74.156397947666,-3.49064704390988,339.777375197464));
#19101=CARTESIAN_POINT('Ctrl Pts',(74.1638069410507,-3.61789982168938,339.684396414298));
#19102=CARTESIAN_POINT('Ctrl Pts',(74.1712159344354,-3.7413517752089,339.586390659074));
#19103=CARTESIAN_POINT('Ctrl Pts',(74.1786249278202,-3.8605984232128,339.483716134769));
#19104=CARTESIAN_POINT('Ctrl Pts',(74.1860384854004,-3.97991853126521,339.380978359415));
#19105=CARTESIAN_POINT('Ctrl Pts',(74.1934520429806,-4.0950278994344,339.273566337949));
#19106=CARTESIAN_POINT('Ctrl Pts',(74.2008656005609,-4.20555925726856,339.161874805434));
#19107=CARTESIAN_POINT('Ctrl Pts',(74.2082897126975,-4.31624797672599,339.050024259573));
#19108=CARTESIAN_POINT('Ctrl Pts',(74.2157138248342,-4.42234541778899,338.933882309191));
#19109=CARTESIAN_POINT('Ctrl Pts',(74.2231379369709,-4.52352437360274,338.813877004299));
#19110=CARTESIAN_POINT('Ctrl Pts',(74.2269950621259,-4.57609091468348,338.751529416911));
#19111=CARTESIAN_POINT('Ctrl Pts',(74.2308521872808,-4.62733055258898,338.688139516362));
#19112=CARTESIAN_POINT('Ctrl Pts',(74.2347093124358,-4.6772021127327,338.623770268539));
#19113=CARTESIAN_POINT('Ctrl Pts',(74.2423589919299,-4.77611035025298,338.496109356502));
#19114=CARTESIAN_POINT('Ctrl Pts',(74.250008671424,-4.86994652241147,338.364191630763));
#19115=CARTESIAN_POINT('Ctrl Pts',(74.2576583509181,-4.95832438822373,338.228459357595));
#19116=CARTESIAN_POINT('Ctrl Pts',(74.265078207762,-5.04404707935131,338.096804948181));
#19117=CARTESIAN_POINT('Ctrl Pts',(74.2724980646059,-5.1246344399638,337.961562210214));
#19118=CARTESIAN_POINT('Ctrl Pts',(74.2799179214499,-5.19977333234696,337.823169823924));
#19119=CARTESIAN_POINT('Ctrl Pts',(74.2873306662723,-5.27484020320359,337.68491008839));
#19120=CARTESIAN_POINT('Ctrl Pts',(74.2947434110947,-5.34446882398607,337.543507037777));
#19121=CARTESIAN_POINT('Ctrl Pts',(74.3021561559172,-5.40838925348953,337.399428316337));
#19122=CARTESIAN_POINT('Ctrl Pts',(74.3095632481942,-5.47226094084134,337.255459461288));
#19123=CARTESIAN_POINT('Ctrl Pts',(74.3169703404712,-5.53043295194006,337.108819335603));
#19124=CARTESIAN_POINT('Ctrl Pts',(74.3243774327482,-5.58268128323765,336.960000064359));
#19125=CARTESIAN_POINT('Ctrl Pts',(74.3317803281464,-5.63490001048733,336.811265114523));
#19126=CARTESIAN_POINT('Ctrl Pts',(74.3391832235446,-5.68120161851954,336.660353827863));
#19127=CARTESIAN_POINT('Ctrl Pts',(74.3465861189427,-5.72141030393377,336.507778066076));
#19128=CARTESIAN_POINT('Ctrl Pts',(74.3539867174594,-5.76160651387961,336.355249643666));
#19129=CARTESIAN_POINT('Ctrl Pts',(74.361387315976,-5.7957134694907,336.20105813341));
#19130=CARTESIAN_POINT('Ctrl Pts',(74.3687879144927,-5.82360530532201,336.045730276087));
#19131=CARTESIAN_POINT('Ctrl Pts',(74.3761872484323,-5.85149237513666,335.890428960407));
#19132=CARTESIAN_POINT('Ctrl Pts',(74.3835865823718,-5.87316637764072,335.733992050929));
#19133=CARTESIAN_POINT('Ctrl Pts',(74.3909859163114,-5.88855265489511,335.576955971481));
#19134=CARTESIAN_POINT('Ctrl Pts',(74.3983864492706,-5.90394142540762,335.419894445236));
#19135=CARTESIAN_POINT('Ctrl Pts',(74.4057869822299,-5.91304040122936,335.262233925485));
#19136=CARTESIAN_POINT('Ctrl Pts',(74.4131875151892,-5.91582682860317,335.104515532238));
#19137=CARTESIAN_POINT('Ctrl Pts',(74.4148922168909,-5.91646867798239,335.068185336178));
#19138=CARTESIAN_POINT('Ctrl Pts',(74.4165969185926,-5.91677579908169,335.031852074546));
#19139=CARTESIAN_POINT('Ctrl Pts',(74.4183016202943,-5.91674830572166,334.995522362246));
#19140=CARTESIAN_POINT('',(76.1683016202944,-5.92582145116702,334.998177799619));
#19141=CARTESIAN_POINT('Ctrl Pts',(74.41830372254,-5.91087398967905,334.995482050269));
#19142=CARTESIAN_POINT('Ctrl Pts',(74.4498515972632,-5.915576218536,334.323813884359));
#19143=CARTESIAN_POINT('Ctrl Pts',(74.574145483411,-5.49945147134948,331.683203449152));
#19144=CARTESIAN_POINT('Ctrl Pts',(74.7911853809838,-1.60867620262318,328.190830902648));
#19145=CARTESIAN_POINT('Ctrl Pts',(75.0694234152574,4.85542856215696,329.962397752996));
#19146=CARTESIAN_POINT('Ctrl Pts',(75.3476614495315,6.86377820144993,336.35689783053));
#19147=CARTESIAN_POINT('Ctrl Pts',(75.6258994838053,2.57333989447748,341.506192796768));
#19148=CARTESIAN_POINT('Ctrl Pts',(75.899446207393,-3.96645730280381,340.698699134842));
#19149=CARTESIAN_POINT('Ctrl Pts',(76.080246919556,-5.91830003067549,336.860747988309));
#19150=CARTESIAN_POINT('Ctrl Pts',(76.1683016202944,-5.92582145116702,334.998177799619));
#19151=CARTESIAN_POINT('',(77.9183016202943,-5.91636786088317,335.005450758099));
#19152=CARTESIAN_POINT('Ctrl Pts',(76.1683016202944,-5.92582145116702,334.998177799619));
#19153=CARTESIAN_POINT('Ctrl Pts',(76.1729929309807,-5.92622217162864,334.898945216272));
#19154=CARTESIAN_POINT('Ctrl Pts',(76.2704302530915,-5.8789467039455,332.838299720819));
#19155=CARTESIAN_POINT('Ctrl Pts',(76.4606135866272,-3.48425963772524,328.932664695425));
#19156=CARTESIAN_POINT('Ctrl Pts',(76.7388516209012,3.21661888179215,328.786628460286));
#19157=CARTESIAN_POINT('Ctrl Pts',(77.0170896551749,6.96565373070174,334.342511577927));
#19158=CARTESIAN_POINT('Ctrl Pts',(77.2953276894491,4.32241096383202,340.501762115993));
#19159=CARTESIAN_POINT('Ctrl Pts',(77.5735657237229,-2.28744454586805,341.612126766086));
#19160=CARTESIAN_POINT('Ctrl Pts',(77.7812237006714,-5.65392581216805,337.912195455118));
#19161=CARTESIAN_POINT('Ctrl Pts',(77.8961356661952,-5.92069250751692,335.476264034432));
#19162=CARTESIAN_POINT('Ctrl Pts',(77.9183016202943,-5.91636786088317,335.005450758099));
#19163=CARTESIAN_POINT('',(79.6683016202943,-5.90709975113901,334.99907110307));
#19164=CARTESIAN_POINT('Ctrl Pts',(77.9183016202943,-5.91636786088317,335.005450758099));
#19165=CARTESIAN_POINT('Ctrl Pts',(77.9888816776198,-5.90259747202661,333.506303557644));
#19166=CARTESIAN_POINT('Ctrl Pts',(78.15220774637,-4.56196104589022,330.015280932936));
#19167=CARTESIAN_POINT('Ctrl Pts',(78.4082798265448,1.31049715735917,328.127211619599));
#19168=CARTESIAN_POINT('Ctrl Pts',(78.6865178608185,6.48865958174404,332.382764864702));
#19169=CARTESIAN_POINT('Ctrl Pts',(78.9647558950927,5.71227488042645,339.040116163141));
#19170=CARTESIAN_POINT('Ctrl Pts',(79.2429939293665,-0.306180165623157,
341.989912490683));
#19171=CARTESIAN_POINT('Ctrl Pts',(79.4775091711004,-5.14206124859087,339.069624867681));
#19172=CARTESIAN_POINT('Ctrl Pts',(79.6192784014097,-5.90563805222993,336.044468030236));
#19173=CARTESIAN_POINT('Ctrl Pts',(79.6683016202943,-5.90709975113901,334.99907110307));
#19174=CARTESIAN_POINT('',(81.4183016202943,-5.91978654872489,334.994924692135));
#19175=CARTESIAN_POINT('Ctrl Pts',(79.6683016202943,-5.90709975113901,334.99907110307));
#19176=CARTESIAN_POINT('Ctrl Pts',(79.7120244128344,-5.90840341009107,334.06670325762));
#19177=CARTESIAN_POINT('Ctrl Pts',(79.848493216799,-5.26054489141,331.158283532971));
#19178=CARTESIAN_POINT('Ctrl Pts',(80.0777080321885,-0.704531368517576,
328.0389470285));
#19179=CARTESIAN_POINT('Ctrl Pts',(80.3559460664623,5.47243560177532,330.640519353683));
#19180=CARTESIAN_POINT('Ctrl Pts',(80.6341841007362,6.62742919334053,337.242722722158));
#19181=CARTESIAN_POINT('Ctrl Pts',(80.9124221350103,1.70052883486869,341.786812551044));
#19182=CARTESIAN_POINT('Ctrl Pts',(81.1737946415294,-4.39368190432037,340.204825231976));
#19183=CARTESIAN_POINT('Ctrl Pts',(81.3424211366242,-5.90516058242414,336.604266515423));
#19184=CARTESIAN_POINT('Ctrl Pts',(81.4183016202943,-5.91978654872489,334.994924692135));
#19185=CARTESIAN_POINT('',(83.1683016202943,-5.92374140024353,335.003591464748));
#19186=CARTESIAN_POINT('Ctrl Pts',(81.4183016202943,-5.91978654872489,334.994924692135));
#19187=CARTESIAN_POINT('Ctrl Pts',(81.4351671480489,-5.92303737988268,334.637225348714));
#19188=CARTESIAN_POINT('Ctrl Pts',(81.5447786872283,-5.73048622156047,332.315977687839));
#19189=CARTESIAN_POINT('Ctrl Pts',(81.7471362378319,-2.66101092507237,328.529169776771));
#19190=CARTESIAN_POINT('Ctrl Pts',(82.025374272106,4.00143348348799,329.260561612978));
#19191=CARTESIAN_POINT('Ctrl Pts',(82.3036123063798,6.99182144531686,335.258951342982));
#19192=CARTESIAN_POINT('Ctrl Pts',(82.5818503406539,3.56591806589121,341.019705247648));
#19193=CARTESIAN_POINT('Ctrl Pts',(82.8600883749277,-3.13237568973752,341.256264497251));
#19194=CARTESIAN_POINT('Ctrl Pts',(83.055572134808,-5.81886229015184,337.388770887391));
#19195=CARTESIAN_POINT('Ctrl Pts',(83.1583098832635,-5.9252530122218,335.21513720506));
#19196=CARTESIAN_POINT('Ctrl Pts',(83.1683016202943,-5.92374140024353,335.003591464748));
#19197=CARTESIAN_POINT('',(84.9183016202943,-5.90863610109609,335.003151912275));
#19198=CARTESIAN_POINT('Ctrl Pts',(83.1683016202943,-5.92374140024353,335.003591464748));
#19199=CARTESIAN_POINT('Ctrl Pts',(83.2510558946881,-5.91122182011041,333.25151230308));
#19200=CARTESIAN_POINT('Ctrl Pts',(83.4265561805065,-4.15954688889828,329.514063221093));
#19201=CARTESIAN_POINT('Ctrl Pts',(83.6948024777495,2.19789854021227,328.35757085637));
#19202=CARTESIAN_POINT('Ctrl Pts',(83.9730405120235,6.77516939239106,333.253660220452));
#19203=CARTESIAN_POINT('Ctrl Pts',(84.2512785462973,5.13496729450675,339.752339824294));
#19204=CARTESIAN_POINT('Ctrl Pts',(84.5295165805716,-1.21751849755278,341.8898673158));
#19205=CARTESIAN_POINT('Ctrl Pts',(84.751857605237,-5.40097549058787,338.545457143259));
#19206=CARTESIAN_POINT('Ctrl Pts',(84.881452618478,-5.91242016185975,335.788429134871));
#19207=CARTESIAN_POINT('Ctrl Pts',(84.9183016202943,-5.90863610109609,335.003151912275));
#19208=CARTESIAN_POINT('',(86.6683016557598,-5.91499694012912,334.995072884561));
#19209=CARTESIAN_POINT('Ctrl Pts',(84.9183016202943,-5.90863610109609,335.003151912275));
#19210=CARTESIAN_POINT('Ctrl Pts',(84.9741986299026,-5.90289598140656,333.811948723774));
#19211=CARTESIAN_POINT('Ctrl Pts',(85.1228416509356,-4.97462503877836,330.636036147798));
#19212=CARTESIAN_POINT('Ctrl Pts',(85.3642306833932,0.211710701760056,328.006588707936));
#19213=CARTESIAN_POINT('Ctrl Pts',(85.642468717667,5.99547756206436,331.393495913769));
#19214=CARTESIAN_POINT('Ctrl Pts',(85.9207067519411,6.27728315676505,338.090038687625));
#19215=CARTESIAN_POINT('Ctrl Pts',(86.1989447862149,0.798518651050066,341.950898566742));
#19216=CARTESIAN_POINT('Ctrl Pts',(86.4481430756662,-4.76473389874006,339.695812636113));
#19217=CARTESIAN_POINT('Ctrl Pts',(86.6045953536925,-5.90157004990948,336.350648623481));
#19218=CARTESIAN_POINT('Ctrl Pts',(86.6683016202943,-5.91219196599268,334.995075975938));
#19219=CARTESIAN_POINT('',(88.4183016202943,-5.92102082817391,334.999137582022));
#19220=CARTESIAN_POINT('Ctrl Pts',(86.6683016778991,-5.91674794688882,334.995070954768));
#19221=CARTESIAN_POINT('Ctrl Pts',(86.6770913492031,-5.91659201877899,334.807897317635));
#19222=CARTESIAN_POINT('Ctrl Pts',(86.6858810205071,-5.90755058647221,334.621105110605));
#19223=CARTESIAN_POINT('Ctrl Pts',(86.6946706918111,-5.88975493954476,334.43544945788));
#19224=CARTESIAN_POINT('Ctrl Pts',(86.7035231249044,-5.87183222453902,334.248468149105));
#19225=CARTESIAN_POINT('Ctrl Pts',(86.7123755579976,-5.84502993007678,334.062639720827));
#19226=CARTESIAN_POINT('Ctrl Pts',(86.7212279910908,-5.80953093661791,333.878714639809));
#19227=CARTESIAN_POINT('Ctrl Pts',(86.7301500921251,-5.77375256891734,333.6933420831));
#19228=CARTESIAN_POINT('Ctrl Pts',(86.7390721931593,-5.72914013624011,333.509902983608));
#19229=CARTESIAN_POINT('Ctrl Pts',(86.7479942941936,-5.67592904703274,333.329143927338));
#19230=CARTESIAN_POINT('Ctrl Pts',(86.7504698143833,-5.6611651337857,333.278990640399));
#19231=CARTESIAN_POINT('Ctrl Pts',(86.7529453345731,-5.64573954508261,333.22904354358));
#19232=CARTESIAN_POINT('Ctrl Pts',(86.7554208547628,-5.62965795197997,333.179318285309));
#19233=CARTESIAN_POINT('Ctrl Pts',(86.762844832201,-5.58142995333242,333.030194397315));
#19234=CARTESIAN_POINT('Ctrl Pts',(86.770268809639,-5.52719989935396,332.882763137558));
#19235=CARTESIAN_POINT('Ctrl Pts',(86.7776927870771,-5.46710380876563,332.737544142601));
#19236=CARTESIAN_POINT('Ctrl Pts',(86.7851080031049,-5.4070786406061,332.592496527906));
#19237=CARTESIAN_POINT('Ctrl Pts',(86.7925232191326,-5.34120135711314,332.449656322658));
#19238=CARTESIAN_POINT('Ctrl Pts',(86.7999384351604,-5.26965788341659,332.309528599995));
#19239=CARTESIAN_POINT('Ctrl Pts',(86.8073465163046,-5.19818324849036,332.169535707522));
#19240=CARTESIAN_POINT('Ctrl Pts',(86.8147545974487,-5.12105344580863,332.032250431909));
#19241=CARTESIAN_POINT('Ctrl Pts',(86.8221626785929,-5.03850263088355,331.898158321081));
#19242=CARTESIAN_POINT('Ctrl Pts',(86.829565245767,-4.95601326003751,331.764166017459));
#19243=CARTESIAN_POINT('Ctrl Pts',(86.8369678129411,-4.86811110595498,331.633362462657));
#19244=CARTESIAN_POINT('Ctrl Pts',(86.8443703801152,-4.77507637811505,331.506208914994));
#19245=CARTESIAN_POINT('Ctrl Pts',(86.8517690498701,-4.68209063265265,331.379122313118));
#19246=CARTESIAN_POINT('Ctrl Pts',(86.8591677196249,-4.58397791500222,331.255682191615));
#19247=CARTESIAN_POINT('Ctrl Pts',(86.8665663893798,-4.48106183499563,331.136321002795));
#19248=CARTESIAN_POINT('Ctrl Pts',(86.8739638385839,-4.37816273294653,331.016979504865));
#19249=CARTESIAN_POINT('Ctrl Pts',(86.8813612877879,-4.27046208468305,330.901715886512));
#19250=CARTESIAN_POINT('Ctrl Pts',(86.888758736992,-4.15832395758744,330.79092974325));
#19251=CARTESIAN_POINT('Ctrl Pts',(86.8961558654556,-4.04619069260545,330.680148403483));
#19252=CARTESIAN_POINT('Ctrl Pts',(86.9035529939192,-3.92962059684443,330.573844415097));
#19253=CARTESIAN_POINT('Ctrl Pts',(86.9109501223827,-3.8090145956135,330.472380496011));
#19254=CARTESIAN_POINT('Ctrl Pts',(86.9183483898194,-3.68839002406911,330.370900954014));
#19255=CARTESIAN_POINT('Ctrl Pts',(86.9257466572562,-3.56372859531484,330.274263205482));
#19256=CARTESIAN_POINT('Ctrl Pts',(86.9331449246929,-3.43546417630343,330.182789556617));
#19257=CARTESIAN_POINT('Ctrl Pts',(86.9405457912187,-3.30715469665277,330.091283772097));
#19258=CARTESIAN_POINT('Ctrl Pts',(86.9479466577446,-3.17524001026643,330.00494591588));
#19259=CARTESIAN_POINT('Ctrl Pts',(86.9553475242704,-3.04018266385231,329.924054774437));
#19260=CARTESIAN_POINT('Ctrl Pts',(86.9627565176553,-2.90497701155974,329.843074806788));
#19261=CARTESIAN_POINT('Ctrl Pts',(86.9701655110401,-2.76662212789234,329.767553690198));
#19262=CARTESIAN_POINT('Ctrl Pts',(86.977574504425,-2.62560548646099,329.697724413804));
#19263=CARTESIAN_POINT('Ctrl Pts',(86.9849880620053,-2.48450197391433,329.627852120168));
#19264=CARTESIAN_POINT('Ctrl Pts',(86.9924016195857,-2.34073377622073,329.5636788054));
#19265=CARTESIAN_POINT('Ctrl Pts',(86.999815177166,-2.19480751753888,329.505388956127));
#19266=CARTESIAN_POINT('Ctrl Pts',(87.0072392893028,-2.04867350611252,329.447016120582));
#19267=CARTESIAN_POINT('Ctrl Pts',(87.0146634014395,-1.90037564839793,329.394543603615));
#19268=CARTESIAN_POINT('Ctrl Pts',(87.0220875135763,-1.75043564479503,329.348106015155));
#19269=CARTESIAN_POINT('Ctrl Pts',(87.0259446387298,-1.67253577626432,329.323979818349));
#19270=CARTESIAN_POINT('Ctrl Pts',(87.0298017638834,-1.5941928345188,329.301481741589));
#19271=CARTESIAN_POINT('Ctrl Pts',(87.0336588890369,-1.51548085109625,329.280625178181));
#19272=CARTESIAN_POINT('Ctrl Pts',(87.0410828664749,-1.36398045487567,329.240481638623));
#19273=CARTESIAN_POINT('Ctrl Pts',(87.0485068439129,-1.21065536931273,329.206301333703));
#19274=CARTESIAN_POINT('Ctrl Pts',(87.0559308213508,-1.0560161754136,329.178251087537));
#19275=CARTESIAN_POINT('Ctrl Pts',(87.0633460373785,-0.901559479029998,
329.150233944882));
#19276=CARTESIAN_POINT('Ctrl Pts',(87.070761253406,-0.745792124940789,329.128332526772));
#19277=CARTESIAN_POINT('Ctrl Pts',(87.0781764694336,-0.589239454681361,
329.112663808857));
#19278=CARTESIAN_POINT('Ctrl Pts',(87.0855845505777,-0.432837418613007,
329.097010167303));
#19279=CARTESIAN_POINT('Ctrl Pts',(87.0929926317218,-0.275651939561479,
329.087577323808));
#19280=CARTESIAN_POINT('Ctrl Pts',(87.1004007128659,-0.118218040117437,
329.08443112985));
#19281=CARTESIAN_POINT('Ctrl Pts',(87.1078032800399,0.0390986783998228,
329.081287277661));
#19282=CARTESIAN_POINT('Ctrl Pts',(87.1152058472139,0.196663077600628,329.084420765329));
#19283=CARTESIAN_POINT('Ctrl Pts',(87.1226084143879,0.353935638096085,329.093845572068));
#19284=CARTESIAN_POINT('Ctrl Pts',(87.1300070841426,0.511125395275907,329.103265416687));
#19285=CARTESIAN_POINT('Ctrl Pts',(87.1374057538974,0.668023248152384,329.118969961363));
#19286=CARTESIAN_POINT('Ctrl Pts',(87.1448044236521,0.824090414503162,329.140921100444));
#19287=CARTESIAN_POINT('Ctrl Pts',(87.1522018728561,0.980131834617748,329.162868618268));
#19288=CARTESIAN_POINT('Ctrl Pts',(87.15959932206,1.13534247096755,329.191060633368));
#19289=CARTESIAN_POINT('Ctrl Pts',(87.166996771264,1.28918927740853,329.225407237777));
#19290=CARTESIAN_POINT('Ctrl Pts',(87.1743938997275,1.44302941332009,329.259752352977));
#19291=CARTESIAN_POINT('Ctrl Pts',(87.1817910281909,1.59550547265486,329.300251445578));
#19292=CARTESIAN_POINT('Ctrl Pts',(87.1891881566544,1.74609547448755,329.346763656411));
#19293=CARTESIAN_POINT('Ctrl Pts',(87.196586424091,1.89670866342128,329.393283028964));
#19294=CARTESIAN_POINT('Ctrl Pts',(87.2039846915276,2.04543486000551,329.445817253133));
#19295=CARTESIAN_POINT('Ctrl Pts',(87.2113829589642,2.19176823977726,329.504175899321));
#19296=CARTESIAN_POINT('Ctrl Pts',(87.21878382549,2.3381530280044,329.562555047515));
#19297=CARTESIAN_POINT('Ctrl Pts',(87.2261846920157,2.48214297930056,329.626762553507));
#19298=CARTESIAN_POINT('Ctrl Pts',(87.2335855585414,2.62325334560855,329.696560319259));
#19299=CARTESIAN_POINT('Ctrl Pts',(87.2409945519262,2.76451866458943,329.766434729631));
#19300=CARTESIAN_POINT('Ctrl Pts',(87.2484035453109,2.90289774905522,329.841911493389));
#19301=CARTESIAN_POINT('Ctrl Pts',(87.2558125386957,3.03793087352768,329.922706767364));
#19302=CARTESIAN_POINT('Ctrl Pts',(87.2632260962759,3.17304718306261,330.003551814015));
#19303=CARTESIAN_POINT('Ctrl Pts',(87.2706396538561,3.3048131137172,330.089721695728));
#19304=CARTESIAN_POINT('Ctrl Pts',(87.2780532114364,3.43279936334925,330.180890217738));
#19305=CARTESIAN_POINT('Ctrl Pts',(87.285477323573,3.56096782483858,330.27218853483));
#19306=CARTESIAN_POINT('Ctrl Pts',(87.2929014357098,3.68534556394649,330.368499477372));
#19307=CARTESIAN_POINT('Ctrl Pts',(87.3003255478464,3.80553706228962,330.469457181524));
#19308=CARTESIAN_POINT('Ctrl Pts',(87.3041826730012,3.86798138466975,330.521908773457));
#19309=CARTESIAN_POINT('Ctrl Pts',(87.308039798156,3.92929635850881,330.575614024287));
#19310=CARTESIAN_POINT('Ctrl Pts',(87.3118969233108,3.98943065837669,330.630517927202));
#19311=CARTESIAN_POINT('Ctrl Pts',(87.3193209007487,4.10517377470132,330.736193869812));
#19312=CARTESIAN_POINT('Ctrl Pts',(87.3267448781867,4.21688972390287,330.846631281051));
#19313=CARTESIAN_POINT('Ctrl Pts',(87.3341688556247,4.32416191534318,330.96149108056));
#19314=CARTESIAN_POINT('Ctrl Pts',(87.3415840716523,4.4313075094577,331.076215328224));
#19315=CARTESIAN_POINT('Ctrl Pts',(87.3489992876799,4.53401953241901,331.195351305386));
#19316=CARTESIAN_POINT('Ctrl Pts',(87.3564145037075,4.63191532445918,331.318520543377));
#19317=CARTESIAN_POINT('Ctrl Pts',(87.3638225848516,4.72971692166116,331.441571268547));
#19318=CARTESIAN_POINT('Ctrl Pts',(87.3712306659957,4.82271128301208,331.568647238415));
#19319=CARTESIAN_POINT('Ctrl Pts',(87.3786387471397,4.91055350117726,331.699334177083));
#19320=CARTESIAN_POINT('Ctrl Pts',(87.3860413143137,4.99833033677514,331.829923843075));
#19321=CARTESIAN_POINT('Ctrl Pts',(87.3934438814877,5.08096245759623,331.964118817828));
#19322=CARTESIAN_POINT('Ctrl Pts',(87.4008464486617,5.15814614332173,332.101472972933));
#19323=CARTESIAN_POINT('Ctrl Pts',(87.4082451184164,5.23528919217407,332.238754811676));
#19324=CARTESIAN_POINT('Ctrl Pts',(87.4156437881712,5.3069893365025,332.37919219368));
#19325=CARTESIAN_POINT('Ctrl Pts',(87.4230424579259,5.3729870541872,332.522311424324));
#19326=CARTESIAN_POINT('Ctrl Pts',(87.4304399071299,5.43897388429783,332.665407044739));
#19327=CARTESIAN_POINT('Ctrl Pts',(87.4378373563338,5.49925999866321,332.811183297147));
#19328=CARTESIAN_POINT('Ctrl Pts',(87.4452348055378,5.55363254095616,332.959143277314));
#19329=CARTESIAN_POINT('Ctrl Pts',(87.4526319340012,5.60800272575043,333.107096842194));
#19330=CARTESIAN_POINT('Ctrl Pts',(87.4600290624647,5.65645971955299,333.257233596266));
#19331=CARTESIAN_POINT('Ctrl Pts',(87.4674261909281,5.69883950001306,333.409038367656));
#19332=CARTESIAN_POINT('Ctrl Pts',(87.4748244583647,5.7412258059014,333.560866513191));
#19333=CARTESIAN_POINT('Ctrl Pts',(87.4822227258013,5.77753293490812,333.714362827944));
#19334=CARTESIAN_POINT('Ctrl Pts',(87.4896209932379,5.8076472927037,333.86899890095));
#19335=CARTESIAN_POINT('Ctrl Pts',(87.4970218597636,5.83777222998987,334.023689299236));
#19336=CARTESIAN_POINT('Ctrl Pts',(87.5044227262893,5.86169999318229,334.179519886889));
#19337=CARTESIAN_POINT('Ctrl Pts',(87.5118235928151,5.8793684790117,334.335954180418));
#19338=CARTESIAN_POINT('Ctrl Pts',(87.5192325861998,5.89705636652772,334.492560253758));
#19339=CARTESIAN_POINT('Ctrl Pts',(87.5266415795845,5.90847120845254,334.649770985798));
#19340=CARTESIAN_POINT('Ctrl Pts',(87.5340505729693,5.9136029107264,334.807046179752));
#19341=CARTESIAN_POINT('Ctrl Pts',(87.5414641305495,5.91873777430587,334.964418260651));
#19342=CARTESIAN_POINT('Ctrl Pts',(87.5488776881297,5.91758178822474,335.121854510262));
#19343=CARTESIAN_POINT('Ctrl Pts',(87.5562912457099,5.91017693659669,335.278817396553));
#19344=CARTESIAN_POINT('Ctrl Pts',(87.5637153578466,5.9027615428067,335.436003748248));
#19345=CARTESIAN_POINT('Ctrl Pts',(87.5711394699833,5.88907954794415,335.592715019877));
#19346=CARTESIAN_POINT('Ctrl Pts',(87.57856358212,5.86922457702474,335.748420621675));
#19347=CARTESIAN_POINT('Ctrl Pts',(87.5824207072749,5.85890912025721,335.829315950625));
#19348=CARTESIAN_POINT('Ctrl Pts',(87.5862778324298,5.84692827967926,335.909940013058));
#19349=CARTESIAN_POINT('Ctrl Pts',(87.5901349575847,5.83330053655822,335.990219880981));
#19350=CARTESIAN_POINT('Ctrl Pts',(87.5975589350227,5.8070706235016,336.144738053001));
#19351=CARTESIAN_POINT('Ctrl Pts',(87.6049829124607,5.77465735868433,336.298446398159));
#19352=CARTESIAN_POINT('Ctrl Pts',(87.6124068898987,5.73612044091608,336.450811100662));
#19353=CARTESIAN_POINT('Ctrl Pts',(87.6198221059263,5.69762900250901,336.602995989892));
#19354=CARTESIAN_POINT('Ctrl Pts',(87.627237321954,5.65302838689777,336.753840034528));
#19355=CARTESIAN_POINT('Ctrl Pts',(87.6346525379816,5.60242977730287,336.902816636697));
#19356=CARTESIAN_POINT('Ctrl Pts',(87.6420606191257,5.55187985343535,337.051649894329));
#19357=CARTESIAN_POINT('Ctrl Pts',(87.6494687002698,5.49534354426832,337.19861893565));
#19358=CARTESIAN_POINT('Ctrl Pts',(87.6568767814139,5.43298257409329,337.343209532265));
#19359=CARTESIAN_POINT('Ctrl Pts',(87.664279348588,5.37066802032726,337.487692507459));
#19360=CARTESIAN_POINT('Ctrl Pts',(87.671681915762,5.30253758513885,337.629800221682));
#19361=CARTESIAN_POINT('Ctrl Pts',(87.679084482936,5.228802066933,337.769035844358));
#19362=CARTESIAN_POINT('Ctrl Pts',(87.6864831526908,5.15510537015528,337.908198160087));
#19363=CARTESIAN_POINT('Ctrl Pts',(87.6938818224455,5.0758096417775,338.044491066806));
#19364=CARTESIAN_POINT('Ctrl Pts',(87.7012804922003,4.99117277940121,338.177439983487));
#19365=CARTESIAN_POINT('Ctrl Pts',(87.7086779414042,4.90654987947903,338.310366967727));
#19366=CARTESIAN_POINT('Ctrl Pts',(87.7160753906082,4.8165877945281,338.439950742262));
#19367=CARTESIAN_POINT('Ctrl Pts',(87.7234728398122,4.72158919314777,338.565743408274));
#19368=CARTESIAN_POINT('Ctrl Pts',(87.7308699682757,4.62659471074119,338.691530620135));
#19369=CARTESIAN_POINT('Ctrl Pts',(87.7382670967392,4.52656437102247,338.813526752482));
#19370=CARTESIAN_POINT('Ctrl Pts',(87.7456642252027,4.42184263110569,338.931315086359));
#19371=CARTESIAN_POINT('Ctrl Pts',(87.7530624926393,4.3171047666551,339.049121556699));
#19372=CARTESIAN_POINT('Ctrl Pts',(87.7604607600759,4.20767431168648,339.162718659589));
#19373=CARTESIAN_POINT('Ctrl Pts',(87.7678590275125,4.09393414584336,339.271724917641));
#19374=CARTESIAN_POINT('Ctrl Pts',(87.7752598940383,3.98015402188385,339.380769470738));
#19375=CARTESIAN_POINT('Ctrl Pts',(87.7826607605641,3.86206144186349,339.48521970982));
#19376=CARTESIAN_POINT('Ctrl Pts',(87.7900616270898,3.74007393855449,339.584733088921));
#19377=CARTESIAN_POINT('Ctrl Pts',(87.7974706204746,3.61795248130439,339.684355743226));
#19378=CARTESIAN_POINT('Ctrl Pts',(87.8048796138594,3.491927848736,339.779030475183));
#19379=CARTESIAN_POINT('Ctrl Pts',(87.8122886072441,3.36244884137766,339.868456465002));
#19380=CARTESIAN_POINT('Ctrl Pts',(87.8197021648244,3.23289007048449,339.957937544316));
#19381=CARTESIAN_POINT('Ctrl Pts',(87.8271157224046,3.09987299903118,340.042163239313));
#19382=CARTESIAN_POINT('Ctrl Pts',(87.8345292799849,2.96387236918584,340.120877965904));
#19383=CARTESIAN_POINT('Ctrl Pts',(87.8419533921216,2.82767811754576,340.199704757318));
#19384=CARTESIAN_POINT('Ctrl Pts',(87.8493775042583,2.68849215345135,340.273004737115));
#19385=CARTESIAN_POINT('Ctrl Pts',(87.856801616395,2.5468113270224,340.340569504));
#19386=CARTESIAN_POINT('Ctrl Pts',(87.8606587415496,2.47320243353146,340.375672120597));
#19387=CARTESIAN_POINT('Ctrl Pts',(87.8645158667041,2.39892041910277,340.409227482542));
#19388=CARTESIAN_POINT('Ctrl Pts',(87.8683729918587,2.32403661171482,340.441211665604));
#19389=CARTESIAN_POINT('Ctrl Pts',(87.8757969692967,2.17990447333581,340.502773021255));
#19390=CARTESIAN_POINT('Ctrl Pts',(87.8832209467346,2.03310716920329,340.558696420712));
#19391=CARTESIAN_POINT('Ctrl Pts',(87.8906449241726,1.88412590285825,340.60874318762));
#19392=CARTESIAN_POINT('Ctrl Pts',(87.8980601402003,1.73532045682294,340.658730891814));
#19393=CARTESIAN_POINT('Ctrl Pts',(87.9054753562279,1.58433652928149,340.702855650617));
#19394=CARTESIAN_POINT('Ctrl Pts',(87.9128905722555,1.43167711524247,340.740925988043));
#19395=CARTESIAN_POINT('Ctrl Pts',(87.9202986533996,1.27916458932299,340.778959694383));
#19396=CARTESIAN_POINT('Ctrl Pts',(87.9277067345437,1.12498014608605,340.810950487196));
#19397=CARTESIAN_POINT('Ctrl Pts',(87.9351148156878,0.96964372945409,340.836756085398));
#19398=CARTESIAN_POINT('Ctrl Pts',(87.9425173828618,0.814422932553928,340.862542476022));
#19399=CARTESIAN_POINT('Ctrl Pts',(87.9499199500358,0.658052236124898,340.882152777878));
#19400=CARTESIAN_POINT('Ctrl Pts',(87.9573225172098,0.501063510710853,340.895495392309));
#19401=CARTESIAN_POINT('Ctrl Pts',(87.9647211869646,0.344157439174849,340.908830981911));
#19402=CARTESIAN_POINT('Ctrl Pts',(87.9721198567193,0.186634357620482,340.915905424529));
#19403=CARTESIAN_POINT('Ctrl Pts',(87.979518526474,0.0290329145482715,340.916678768733));
#19404=CARTESIAN_POINT('Ctrl Pts',(87.986915975678,-0.128542529179842,340.917451985358));
#19405=CARTESIAN_POINT('Ctrl Pts',(87.994313424882,-0.28619593592554,340.911926164783));
#19406=CARTESIAN_POINT('Ctrl Pts',(88.001710874086,-0.443386866669154,340.900113443737));
#19407=CARTESIAN_POINT('Ctrl Pts',(88.0091080025494,-0.600570981888055,
340.88830123487));
#19408=CARTESIAN_POINT('Ctrl Pts',(88.0165051310129,-0.757292288813252,
340.870202695496));
#19409=CARTESIAN_POINT('Ctrl Pts',(88.0239022594764,-0.913013954075224,
340.845881976414));
#19410=CARTESIAN_POINT('Ctrl Pts',(88.031300526913,-1.06875959658631,340.821557512548));
#19411=CARTESIAN_POINT('Ctrl Pts',(88.0386987943496,-1.22350492219589,340.791009018943));
#19412=CARTESIAN_POINT('Ctrl Pts',(88.0460970617862,-1.37672194028502,340.754352027956));
#19413=CARTESIAN_POINT('Ctrl Pts',(88.0534979283119,-1.52999278512387,340.717682158982));
#19414=CARTESIAN_POINT('Ctrl Pts',(88.0608987948377,-1.68173389071534,340.674899606769));
#19415=CARTESIAN_POINT('Ctrl Pts',(88.0682996613634,-1.83143125190803,340.626170112255));
#19416=CARTESIAN_POINT('Ctrl Pts',(88.0757086547482,-1.98129299511505,340.577387108098));
#19417=CARTESIAN_POINT('Ctrl Pts',(88.0831176481329,-2.12910615698859,340.522644235851));
#19418=CARTESIAN_POINT('Ctrl Pts',(88.0905266415177,-2.27437490003277,340.462156110603));
#19419=CARTESIAN_POINT('Ctrl Pts',(88.0979401990979,-2.41973313363353,340.401630722584));
#19420=CARTESIAN_POINT('Ctrl Pts',(88.1053537566782,-2.56254348731432,340.335353185837));
#19421=CARTESIAN_POINT('Ctrl Pts',(88.1127673142584,-2.7023341247331,340.263584409963));
#19422=CARTESIAN_POINT('Ctrl Pts',(88.1201914263951,-2.84232377971634,340.191713458097));
#19423=CARTESIAN_POINT('Ctrl Pts',(88.1276155385318,-2.9792848081739,340.114335836508));
#19424=CARTESIAN_POINT('Ctrl Pts',(88.1350396506685,-3.11277308690336,340.031756579163));
#19425=CARTESIAN_POINT('Ctrl Pts',(88.1388967758232,-3.18212562203004,339.988853330277));
#19426=CARTESIAN_POINT('Ctrl Pts',(88.1427539009779,-3.25054130207272,339.944546731359));
#19427=CARTESIAN_POINT('Ctrl Pts',(88.1466110261326,-3.31796140897478,339.898883816856));
#19428=CARTESIAN_POINT('Ctrl Pts',(88.1540056697473,-3.44721510000488,339.811341679741));
#19429=CARTESIAN_POINT('Ctrl Pts',(88.161400313362,-3.57320442184648,339.718543326015));
#19430=CARTESIAN_POINT('Ctrl Pts',(88.1687949569768,-3.69547034580423,339.620760704233));
#19431=CARTESIAN_POINT('Ctrl Pts',(88.1761808557596,-3.81759167929758,339.523093719206));
#19432=CARTESIAN_POINT('Ctrl Pts',(88.1835667545425,-3.93599808729685,339.420454430029));
#19433=CARTESIAN_POINT('Ctrl Pts',(88.1909526533253,-4.05025826768325,339.313158764475));
#19434=CARTESIAN_POINT('Ctrl Pts',(88.1983314614447,-4.16440875519343,339.205966105673));
#19435=CARTESIAN_POINT('Ctrl Pts',(88.2057102695642,-4.27442066581368,339.094126224688));
#19436=CARTESIAN_POINT('Ctrl Pts',(88.2130890776836,-4.37989476856159,338.977996025492));
#19437=CARTESIAN_POINT('Ctrl Pts',(88.2204624434414,-4.48529107714643,338.861951480037));
#19438=CARTESIAN_POINT('Ctrl Pts',(88.2278358091993,-4.58615598917958,338.741623193864));
#19439=CARTESIAN_POINT('Ctrl Pts',(88.2352091749572,-4.68212635611665,338.617405610083));
#19440=CARTESIAN_POINT('Ctrl Pts',(88.2428380268462,-4.78142208335221,338.488883903741));
#19441=CARTESIAN_POINT('Ctrl Pts',(88.2504668787353,-4.87547766557774,338.356198801304));
#19442=CARTESIAN_POINT('Ctrl Pts',(88.2580957306243,-4.96393512596535,338.219825869159));
#19443=CARTESIAN_POINT('Ctrl Pts',(88.2654641718353,-5.04937309304298,338.088108023816));
#19444=CARTESIAN_POINT('Ctrl Pts',(88.2728326130462,-5.12958862495197,337.952950321232));
#19445=CARTESIAN_POINT('Ctrl Pts',(88.2802010542572,-5.20430267079867,337.814811587517));
#19446=CARTESIAN_POINT('Ctrl Pts',(88.2875693652775,-5.27901539654684,337.676675294531));
#19447=CARTESIAN_POINT('Ctrl Pts',(88.2949376762978,-5.34822665016277,337.535558406234));
#19448=CARTESIAN_POINT('Ctrl Pts',(88.3023059873182,-5.41170317014393,337.391944681792));
#19449=CARTESIAN_POINT('Ctrl Pts',(88.3096756524486,-5.47519135551132,337.248304564763));
#19450=CARTESIAN_POINT('Ctrl Pts',(88.3170453175789,-5.53294255713081,337.102167042566));
#19451=CARTESIAN_POINT('Ctrl Pts',(88.3244149827093,-5.58477160117974,336.954036009176));
#19452=CARTESIAN_POINT('Ctrl Pts',(88.331787486827,-5.63662061112845,336.805847911848));
#19453=CARTESIAN_POINT('Ctrl Pts',(88.3391599909446,-5.68254279796302,336.655665129711));
#19454=CARTESIAN_POINT('Ctrl Pts',(88.3465324950622,-5.72240285811786,336.504006679475));
#19455=CARTESIAN_POINT('Ctrl Pts',(88.3539130925853,-5.76230667594628,336.352181741256));
#19456=CARTESIAN_POINT('Ctrl Pts',(88.3612936901084,-5.79613498510369,336.198878264866));
#19457=CARTESIAN_POINT('Ctrl Pts',(88.3686742876315,-5.82380348353425,336.044626032451));
#19458=CARTESIAN_POINT('Ctrl Pts',(88.3760597134761,-5.85149008245112,335.890272889594));
#19459=CARTESIAN_POINT('Ctrl Pts',(88.3834451393207,-5.87300879162604,335.734970125933));
#19460=CARTESIAN_POINT('Ctrl Pts',(88.3908305651652,-5.88832723993724,335.579251998627));
#19461=CARTESIAN_POINT('Ctrl Pts',(88.3982258965774,-5.90366623383771,335.423325017224));
#19462=CARTESIAN_POINT('Ctrl Pts',(88.4056212279896,-5.91278834517379,335.266981934148));
#19463=CARTESIAN_POINT('Ctrl Pts',(88.4130165594018,-5.91571326754579,335.110756935145));
#19464=CARTESIAN_POINT('Ctrl Pts',(88.4147782463659,-5.91641003112903,335.073541626069));
#19465=CARTESIAN_POINT('Ctrl Pts',(88.4165399333301,-5.91675535479303,335.03633299364));
#19466=CARTESIAN_POINT('Ctrl Pts',(88.4183016202943,-5.91674993723816,334.999138204092));
#19467=CARTESIAN_POINT('',(90.1683016202942,-5.91477476057368,335.005386709628));
#19468=CARTESIAN_POINT('Ctrl Pts',(88.4183016202943,-5.92634586416711,334.999136806411));
#19469=CARTESIAN_POINT('Ctrl Pts',(88.4204841003317,-5.92643975629784,334.952982996016));
#19470=CARTESIAN_POINT('Ctrl Pts',(88.4226665803691,-5.9259473617588,334.906831241244));
#19471=CARTESIAN_POINT('Ctrl Pts',(88.5175950718312,-5.87876314062022,332.900034320683));
#19472=CARTESIAN_POINT('Ctrl Pts',(88.7030870946803,-3.64692550512862,329.029023758107));
#19473=CARTESIAN_POINT('Ctrl Pts',(88.9813251289543,3.0475606556344,328.70198467996));
#19474=CARTESIAN_POINT('Ctrl Pts',(89.2595631632284,6.94534538464283,334.154541302462));
#19475=CARTESIAN_POINT('Ctrl Pts',(89.5378011975022,4.46948916729357,340.382962892745));
#19476=CARTESIAN_POINT('Ctrl Pts',(89.8160392317763,-2.10795128932855,341.671518888756));
#19477=CARTESIAN_POINT('Ctrl Pts',(90.0262060393735,-5.61504000227453,338.020314320455));
#19478=CARTESIAN_POINT('Ctrl Pts',(90.1436268355462,-5.91942493170759,335.529848181018));
#19479=CARTESIAN_POINT('Ctrl Pts',(90.1683016202942,-5.91477476057368,335.005386709628));
#19480=CARTESIAN_POINT('',(91.9183016202943,-5.90746550964324,334.998215606661));
#19481=CARTESIAN_POINT('Ctrl Pts',(90.1683016202942,-5.91477476057368,335.005386709628));
#19482=CARTESIAN_POINT('Ctrl Pts',(90.2363728469709,-5.90194616423239,333.558535761722));
#19483=CARTESIAN_POINT('Ctrl Pts',(90.3971900850721,-4.63796763427977,330.120318055911));
#19484=CARTESIAN_POINT('Ctrl Pts',(90.6507533345981,1.12431756930355,328.094311553177));
#19485=CARTESIAN_POINT('Ctrl Pts',(90.9289913688719,6.4155734914137,332.208398363396));
#19486=CARTESIAN_POINT('Ctrl Pts',(91.2072294031458,5.81935231416251,338.884296791552));
#19487=CARTESIAN_POINT('Ctrl Pts',(91.4854674374199,-0.117202588295501,
341.995633386228));
#19488=CARTESIAN_POINT('Ctrl Pts',(91.7224915098026,-5.08278279076532,339.177244506712));
#19489=CARTESIAN_POINT('Ctrl Pts',(91.8667695707608,-5.90450367428727,336.096942434057));
#19490=CARTESIAN_POINT('Ctrl Pts',(91.9183016202943,-5.90746550964324,334.998215606661));
#19491=CARTESIAN_POINT('',(93.6683016202942,-5.92133609402893,334.995342413241));
#19492=CARTESIAN_POINT('Ctrl Pts',(91.9183016202943,-5.90746550964324,334.998215606661));
#19493=CARTESIAN_POINT('Ctrl Pts',(91.9595155821854,-5.90983430674317,334.119483128464));
#19494=CARTESIAN_POINT('Ctrl Pts',(92.0934755555012,-5.31350020957016,331.266347748298));
#19495=CARTESIAN_POINT('Ctrl Pts',(92.3201815402416,-0.892360157151169,
328.060524784164));
#19496=CARTESIAN_POINT('Ctrl Pts',(92.5984195745155,5.35264547155506,330.494247079894));
#19497=CARTESIAN_POINT('Ctrl Pts',(92.8766576087896,6.68560735593236,337.062832325594));
#19498=CARTESIAN_POINT('Ctrl Pts',(93.1548956430633,1.88328604917356,341.738386793456));
#19499=CARTESIAN_POINT('Ctrl Pts',(93.4187769802319,-4.31032992291039,340.308042313538));
#19500=CARTESIAN_POINT('Ctrl Pts',(93.5899123059753,-5.90699168792046,336.656767378768));
#19501=CARTESIAN_POINT('Ctrl Pts',(93.6683016202942,-5.92133609402893,334.995342413241));
#19502=CARTESIAN_POINT('',(95.4183016202943,-5.92241488864615,335.004254353173));
#19503=CARTESIAN_POINT('Ctrl Pts',(93.6683016202942,-5.92133609402893,334.995342413241));
#19504=CARTESIAN_POINT('Ctrl Pts',(93.6826583173999,-5.9239632160474,334.691058912344));
#19505=CARTESIAN_POINT('Ctrl Pts',(93.7897610259302,-5.76414273014026,332.423834031691));
#19506=CARTESIAN_POINT('Ctrl Pts',(93.9896097458853,-2.83487969874721,328.603432169137));
#19507=CARTESIAN_POINT('Ctrl Pts',(94.2678477801593,3.844894283409,329.15453929355));
#19508=CARTESIAN_POINT('Ctrl Pts',(94.546085814433,6.99626553222726,335.069939429418));
#19509=CARTESIAN_POINT('Ctrl Pts',(94.8243238487073,3.72726716683056,340.921157183209));
#19510=CARTESIAN_POINT('Ctrl Pts',(95.1025618829809,-2.96218926319552,341.338616386109));
#19511=CARTESIAN_POINT('Ctrl Pts',(95.30055447351,-5.78800059838624,337.496437496031));
#19512=CARTESIAN_POINT('Ctrl Pts',(95.4058010526145,-5.92456336273099,335.269072437427));
#19513=CARTESIAN_POINT('Ctrl Pts',(95.4183016202943,-5.92241488864615,335.004254353173));
#19514=CARTESIAN_POINT('',(97.1683016202942,-5.90788275435609,335.002389220978));
#19515=CARTESIAN_POINT('Ctrl Pts',(95.4183016202943,-5.92241488864615,335.004254353173));
#19516=CARTESIAN_POINT('Ctrl Pts',(95.4985470640392,-5.90862309448696,333.304295981126));
#19517=CARTESIAN_POINT('Ctrl Pts',(95.6715385192085,-4.24711155794473,329.616037147329));
#19518=CARTESIAN_POINT('Ctrl Pts',(95.9372759858029,2.01761921385354,328.300609309115));
#19519=CARTESIAN_POINT('Ctrl Pts',(96.2155140200769,6.72551008477971,333.071234327155));
#19520=CARTESIAN_POINT('Ctrl Pts',(96.4937520543506,5.26149961926853,339.611859134628));
#19521=CARTESIAN_POINT('Ctrl Pts',(96.7719900886248,-1.03091138723976,341.920248885184));
#19522=CARTESIAN_POINT('Ctrl Pts',(96.9968399439392,-5.35141349029995,338.653647685618));
#19523=CARTESIAN_POINT('Ctrl Pts',(97.128943787829,-5.91092380235256,335.841398759276));
#19524=CARTESIAN_POINT('Ctrl Pts',(97.1683016202942,-5.90788275435609,335.002389220978));
#19525=CARTESIAN_POINT('',(98.9183016202944,-5.91363949802178,334.994757320841));
#19526=CARTESIAN_POINT('Ctrl Pts',(97.1683016202942,-5.90788275435609,335.002389220978));
#19527=CARTESIAN_POINT('Ctrl Pts',(97.2216897992537,-5.90375762844111,333.864288147476));
#19528=CARTESIAN_POINT('Ctrl Pts',(97.3678239896376,-5.03757698457894,330.743267499416));
#19529=CARTESIAN_POINT('Ctrl Pts',(97.6067041914465,0.0226730784917184,
328.003421632488));
#19530=CARTESIAN_POINT('Ctrl Pts',(97.8849422257205,5.89584171844692,331.23281625717));
#19531=CARTESIAN_POINT('Ctrl Pts',(98.1631802599943,6.35848343586405,337.919299799106));
#19532=CARTESIAN_POINT('Ctrl Pts',(98.4414182942685,0.986038755248901,341.926785004198));
#19533=CARTESIAN_POINT('Ctrl Pts',(98.6931254143681,-4.69271617403346,339.801658490069));
#19534=CARTESIAN_POINT('Ctrl Pts',(98.8520865230436,-5.90167453875089,336.402842058547));
#19535=CARTESIAN_POINT('Ctrl Pts',(98.9183016202944,-5.91363949802178,334.994757320841));
#19536=CARTESIAN_POINT('',(100.668301620294,-5.92209910998399,335.000129634886));
#19537=CARTESIAN_POINT('Ctrl Pts',(98.9183016202944,-5.91363949802178,334.994757320841));
#19538=CARTESIAN_POINT('Ctrl Pts',(98.9448325344683,-5.91843359061835,334.430569139038));
#19539=CARTESIAN_POINT('Ctrl Pts',(99.064109460067,-5.58514965359588,331.89965766233));
#19540=CARTESIAN_POINT('Ctrl Pts',(99.2761323970899,-1.97415726733455,328.287673577286));
#19541=CARTESIAN_POINT('Ctrl Pts',(99.5543704313643,4.57620871558837,329.707464056562));
#19542=CARTESIAN_POINT('Ctrl Pts',(99.8326084656378,6.92705550494563,335.984136653425));
#19543=CARTESIAN_POINT('Ctrl Pts',(100.110846499912,2.92104570058681,341.357681569276));
#19544=CARTESIAN_POINT('Ctrl Pts',(100.389084534186,-3.7655646286397,340.896875948225));
#19545=CARTESIAN_POINT('Ctrl Pts',(100.574902907646,-5.92335917044606,336.975133811572));
#19546=CARTESIAN_POINT('Ctrl Pts',(100.667975269683,-5.92649868725284,335.007030730633));
#19547=CARTESIAN_POINT('Ctrl Pts',(100.668301620294,-5.9264964672619,335.000129731144));
#19548=CARTESIAN_POINT('',(102.418301603228,-5.91452397649362,335.005174647363));
#19549=CARTESIAN_POINT('Ctrl Pts',(100.668301620294,-5.91674999858243,335.000129517794));
#19550=CARTESIAN_POINT('Ctrl Pts',(100.675720896014,-5.91675342721131,334.843499765313));
#19551=CARTESIAN_POINT('Ctrl Pts',(100.683140171735,-5.91053304525965,334.686632128746));
#19552=CARTESIAN_POINT('Ctrl Pts',(100.690559447455,-5.89805807963226,334.530062289463));
#19553=CARTESIAN_POINT('Ctrl Pts',(100.697969965162,-5.88559783996035,334.37367727157));
#19554=CARTESIAN_POINT('Ctrl Pts',(100.705380482868,-5.86689774197576,334.21758972017));
#19555=CARTESIAN_POINT('Ctrl Pts',(100.712791000575,-5.84197897812579,334.062336850657));
#19556=CARTESIAN_POINT('Ctrl Pts',(100.720194391435,-5.81708417915823,333.907233290988));
#19557=CARTESIAN_POINT('Ctrl Pts',(100.727597782296,-5.78598267919092,333.752963181704));
#19558=CARTESIAN_POINT('Ctrl Pts',(100.735001173157,-5.74874757126554,333.600060028298));
#19559=CARTESIAN_POINT('Ctrl Pts',(100.742399062695,-5.71154013205687,333.447270494384));
#19560=CARTESIAN_POINT('Ctrl Pts',(100.749796952234,-5.66820824793961,333.295846255444));
#19561=CARTESIAN_POINT('Ctrl Pts',(100.757194841772,-5.61887630923833,333.146311896791));
#19562=CARTESIAN_POINT('Ctrl Pts',(100.764588851133,-5.56957024503566,332.996855968595));
#19563=CARTESIAN_POINT('Ctrl Pts',(100.771982860494,-5.51427051040527,332.849288300652));
#19564=CARTESIAN_POINT('Ctrl Pts',(100.779376869855,-5.45315165777585,332.704119436949));
#19565=CARTESIAN_POINT('Ctrl Pts',(100.786769683007,-5.39204269301176,332.5589740588));
#19566=CARTESIAN_POINT('Ctrl Pts',(100.794162496158,-5.32511662334934,332.416227058893));
#19567=CARTESIAN_POINT('Ctrl Pts',(100.801555309309,-5.25259660839953,332.276370173476));
#19568=CARTESIAN_POINT('Ctrl Pts',(100.808947825895,-5.1800795026167,332.136518898469));
#19569=CARTESIAN_POINT('Ctrl Pts',(100.816340342481,-5.10196906974435,331.999557839246));
#19570=CARTESIAN_POINT('Ctrl Pts',(100.823732859067,-5.01853488551264,331.865954983509));
#19571=CARTESIAN_POINT('Ctrl Pts',(100.831126542949,-4.93508752681557,331.732331031549));
#19572=CARTESIAN_POINT('Ctrl Pts',(100.838520226832,-4.84631494099473,331.602066655894));
#19573=CARTESIAN_POINT('Ctrl Pts',(100.845913910714,-4.75253047668514,331.475601522149));
#19574=CARTESIAN_POINT('Ctrl Pts',(100.85331022618,-4.6587126323147,331.349091376537));
#19575=CARTESIAN_POINT('Ctrl Pts',(100.860706541646,-4.55987958041388,331.226383465064));
#19576=CARTESIAN_POINT('Ctrl Pts',(100.868102857112,-4.45638533814684,331.10788485776));
#19577=CARTESIAN_POINT('Ctrl Pts',(100.875507300596,-4.35277736315245,330.989256029012));
#19578=CARTESIAN_POINT('Ctrl Pts',(100.88291174408,-4.24449821463794,330.874846023532));
#19579=CARTESIAN_POINT('Ctrl Pts',(100.890316187565,-4.13193969584835,330.765025984451));
#19580=CARTESIAN_POINT('Ctrl Pts',(100.897725232323,-4.01931123086899,330.655137700929));
#19581=CARTESIAN_POINT('Ctrl Pts',(100.905134277082,-3.90239837387915,330.549845316645));
#19582=CARTESIAN_POINT('Ctrl Pts',(100.91254332184,-3.78162604762161,330.449479700249));
#19583=CARTESIAN_POINT('Ctrl Pts',(100.919962843036,-3.66068294852313,330.34897216623));
#19584=CARTESIAN_POINT('Ctrl Pts',(100.927382364231,-3.53586977740861,330.253405539145));
#19585=CARTESIAN_POINT('Ctrl Pts',(100.934801885426,-3.40764109227606,330.163067837076));
#19586=CARTESIAN_POINT('Ctrl Pts',(100.938388124529,-3.34566152343086,330.119402944006));
#19587=CARTESIAN_POINT('Ctrl Pts',(100.941974363632,-3.2828843764741,330.076959000909));
#19588=CARTESIAN_POINT('Ctrl Pts',(100.945560602734,-3.21936296038802,330.035764641782));
#19589=CARTESIAN_POINT('Ctrl Pts',(100.952984580172,-3.0878654371213,329.950487005804));
#19590=CARTESIAN_POINT('Ctrl Pts',(100.96040855761,-2.95277882722675,329.870309185089));
#19591=CARTESIAN_POINT('Ctrl Pts',(100.967832535048,-2.81453648987602,329.795548548631));
#19592=CARTESIAN_POINT('Ctrl Pts',(100.975247751076,-2.67645729928305,329.720876140972));
#19593=CARTESIAN_POINT('Ctrl Pts',(100.982662967104,-2.53523011946853,329.651608367824));
#19594=CARTESIAN_POINT('Ctrl Pts',(100.990078183131,-2.39131784369694,329.588019814068));
#19595=CARTESIAN_POINT('Ctrl Pts',(100.997486264275,-2.24754403959239,329.524492444899));
#19596=CARTESIAN_POINT('Ctrl Pts',(101.004894345419,-2.10109062205886,329.466633566117));
#19597=CARTESIAN_POINT('Ctrl Pts',(101.012302426563,-1.95244558778982,329.414672186056));
#19598=CARTESIAN_POINT('Ctrl Pts',(101.019704993737,-1.8039111927349,329.362749481799));
#19599=CARTESIAN_POINT('Ctrl Pts',(101.027107560911,-1.65318877981853,329.316715658526));
#19600=CARTESIAN_POINT('Ctrl Pts',(101.034510128085,-1.50078675479425,329.276751824433));
#19601=CARTESIAN_POINT('Ctrl Pts',(101.04190879784,-1.34846496877008,329.236809031124));
#19602=CARTESIAN_POINT('Ctrl Pts',(101.049307467595,-1.19446569188727,329.202929956752));
#19603=CARTESIAN_POINT('Ctrl Pts',(101.05670613735,-1.03931283078175,329.175245979248));
#19604=CARTESIAN_POINT('Ctrl Pts',(101.064103586553,-0.884185565080336,
329.14756656874));
#19605=CARTESIAN_POINT('Ctrl Pts',(101.071501035757,-0.727905459902505,
329.126080292255));
#19606=CARTESIAN_POINT('Ctrl Pts',(101.078898484961,-0.571007083957664,
329.110867511036));
#19607=CARTESIAN_POINT('Ctrl Pts',(101.086295613425,-0.414115510852758,
329.095655389416));
#19608=CARTESIAN_POINT('Ctrl Pts',(101.093692741888,-0.256606091751522,
329.086716258238));
#19609=CARTESIAN_POINT('Ctrl Pts',(101.101089870352,-0.0990187279253847,
329.084078613266));
#19610=CARTESIAN_POINT('Ctrl Pts',(101.108488137788,0.0585929004215468,
329.081440562162));
#19611=CARTESIAN_POINT('Ctrl Pts',(101.115886405225,0.216282124208303,329.085105935448));
#19612=CARTESIAN_POINT('Ctrl Pts',(101.123284672662,0.373508977772477,329.095051092006));
#19613=CARTESIAN_POINT('Ctrl Pts',(101.130685539187,0.530791066783069,329.104999742401));
#19614=CARTESIAN_POINT('Ctrl Pts',(101.138086405713,0.687610089929971,329.121232544971));
#19615=CARTESIAN_POINT('Ctrl Pts',(101.145487272239,0.843431284659256,329.143673998951));
#19616=CARTESIAN_POINT('Ctrl Pts',(101.152896265623,0.999423585957447,329.166140095794));
#19617=CARTESIAN_POINT('Ctrl Pts',(101.160305259008,1.15441550102438,329.194828406111));
#19618=CARTESIAN_POINT('Ctrl Pts',(101.167714252393,1.30788181908319,329.229612169896));
#19619=CARTESIAN_POINT('Ctrl Pts',(101.175127809973,1.46144267768766,329.26441736168));
#19620=CARTESIAN_POINT('Ctrl Pts',(101.182541367553,1.61347570701675,329.305325392538));
#19621=CARTESIAN_POINT('Ctrl Pts',(101.189954925134,1.76347143648926,329.352159788451));
#19622=CARTESIAN_POINT('Ctrl Pts',(101.19737903727,1.91368071234296,329.399060861701));
#19623=CARTESIAN_POINT('Ctrl Pts',(101.204803149407,2.06184654494781,329.451905025877));
#19624=CARTESIAN_POINT('Ctrl Pts',(101.212227261544,2.20747923205516,329.510467597095));
#19625=CARTESIAN_POINT('Ctrl Pts',(101.216084386698,2.28314127627484,329.54089321061));
#19626=CARTESIAN_POINT('Ctrl Pts',(101.219941511853,2.35811996050561,329.572861583952));
#19627=CARTESIAN_POINT('Ctrl Pts',(101.223798637008,2.43234939516805,329.606336404416));
#19628=CARTESIAN_POINT('Ctrl Pts',(101.231222614445,2.57522203374634,329.67076685505));
#19629=CARTESIAN_POINT('Ctrl Pts',(101.238646591883,2.71574838958606,329.740975247866));
#19630=CARTESIAN_POINT('Ctrl Pts',(101.246070569321,2.85342706481585,329.816768908463));
#19631=CARTESIAN_POINT('Ctrl Pts',(101.253485785349,2.99094325849408,329.892473121137));
#19632=CARTESIAN_POINT('Ctrl Pts',(101.260901001377,3.12561813730881,329.973749302958));
#19633=CARTESIAN_POINT('Ctrl Pts',(101.268316217404,3.25697029886916,330.06035679074));
#19634=CARTESIAN_POINT('Ctrl Pts',(101.275724298548,3.38819607404093,330.146880945234));
#19635=CARTESIAN_POINT('Ctrl Pts',(101.283132379693,3.51610518729618,330.238725989234));
#19636=CARTESIAN_POINT('Ctrl Pts',(101.290540460837,3.64024097762993,330.335605485459));
#19637=CARTESIAN_POINT('Ctrl Pts',(101.297943028011,3.76428437142794,330.432412872505));
#19638=CARTESIAN_POINT('Ctrl Pts',(101.305345595185,3.88455974158668,330.534247021855));
#19639=CARTESIAN_POINT('Ctrl Pts',(101.312748162359,4.00063966283354,330.640778412301));
#19640=CARTESIAN_POINT('Ctrl Pts',(101.320146832113,4.1166584685091,330.747253714435));
#19641=CARTESIAN_POINT('Ctrl Pts',(101.327545501868,4.22848595012491,330.858421080673));
#19642=CARTESIAN_POINT('Ctrl Pts',(101.334944171623,4.33572811323378,330.973911042884));
#19643=CARTESIAN_POINT('Ctrl Pts',(101.342341620827,4.4429525847157,331.089381952837));
#19644=CARTESIAN_POINT('Ctrl Pts',(101.349739070031,4.54559298526312,331.209173770283));
#19645=CARTESIAN_POINT('Ctrl Pts',(101.357136519235,4.64329245159145,331.332880453068));
#19646=CARTESIAN_POINT('Ctrl Pts',(101.364533647698,4.74098768184118,331.456581772146));
#19647=CARTESIAN_POINT('Ctrl Pts',(101.371930776162,4.83374217252105,331.584197326176));
#19648=CARTESIAN_POINT('Ctrl Pts',(101.379327904625,4.92123978937726,331.715288521354));
#19649=CARTESIAN_POINT('Ctrl Pts',(101.386726172062,5.00875087868236,331.846399901303));
#19650=CARTESIAN_POINT('Ctrl Pts',(101.394124439498,5.0910032752848,331.980987677541));
#19651=CARTESIAN_POINT('Ctrl Pts',(101.401522706935,5.16772465310335,332.118584987856));
#19652=CARTESIAN_POINT('Ctrl Pts',(101.408923573461,5.24447298394842,332.256230637553));
#19653=CARTESIAN_POINT('Ctrl Pts',(101.416324439987,5.31568624565405,332.396887600612));
#19654=CARTESIAN_POINT('Ctrl Pts',(101.423725306512,5.3811385377205,332.540065325998));
#19655=CARTESIAN_POINT('Ctrl Pts',(101.431134299897,5.44666270266144,332.683400274215));
#19656=CARTESIAN_POINT('Ctrl Pts',(101.438543293282,5.50641310915466,332.829261173049));
#19657=CARTESIAN_POINT('Ctrl Pts',(101.445952286667,5.56021213070599,332.977137764441));
#19658=CARTESIAN_POINT('Ctrl Pts',(101.453365844247,5.61404429431039,333.125105452914));
#19659=CARTESIAN_POINT('Ctrl Pts',(101.460779401827,5.66191765425009,333.27509095356));
#19660=CARTESIAN_POINT('Ctrl Pts',(101.468192959407,5.7037049075299,333.426570341477));
#19661=CARTESIAN_POINT('Ctrl Pts',(101.475617071544,5.74555165261478,333.578265388035));
#19662=CARTESIAN_POINT('Ctrl Pts',(101.483041183681,5.78129490135454,333.731458207084));
#19663=CARTESIAN_POINT('Ctrl Pts',(101.490465295817,5.81085858923555,333.885615408215));
#19664=CARTESIAN_POINT('Ctrl Pts',(101.494322420972,5.82621811534386,333.965706280676));
#19665=CARTESIAN_POINT('Ctrl Pts',(101.498179546127,5.83991049649889,334.04605737701));
#19666=CARTESIAN_POINT('Ctrl Pts',(101.502036671282,5.85193061219721,334.126593638374));
#19667=CARTESIAN_POINT('Ctrl Pts',(101.50946064872,5.8750662544607,334.281605302065));
#19668=CARTESIAN_POINT('Ctrl Pts',(101.516884626158,5.89207339365728,334.437770702599));
#19669=CARTESIAN_POINT('Ctrl Pts',(101.524308603596,5.90284271864182,334.594563936635));
#19670=CARTESIAN_POINT('Ctrl Pts',(101.531723819624,5.91359933420257,334.751172131063));
#19671=CARTESIAN_POINT('Ctrl Pts',(101.539139035651,5.91813276352719,334.908406315432));
#19672=CARTESIAN_POINT('Ctrl Pts',(101.546554251679,5.91638487096705,335.06573143154));
#19673=CARTESIAN_POINT('Ctrl Pts',(101.553962332823,5.91463866022033,335.222905170212));
#19674=CARTESIAN_POINT('Ctrl Pts',(101.561370413967,5.90662316389853,335.380169295746));
#19675=CARTESIAN_POINT('Ctrl Pts',(101.568778495111,5.89233212774909,335.536984784511));
#19676=CARTESIAN_POINT('Ctrl Pts',(101.576181062285,5.87805172867886,335.693683552643));
#19677=CARTESIAN_POINT('Ctrl Pts',(101.583583629459,5.85750512414643,335.849933978827));
#19678=CARTESIAN_POINT('Ctrl Pts',(101.590986196633,5.83073811122401,336.005198309201));
#19679=CARTESIAN_POINT('Ctrl Pts',(101.598384866388,5.80398519101701,336.160380893582));
#19680=CARTESIAN_POINT('Ctrl Pts',(101.605783536143,5.77101844805768,336.31457804926));
#19681=CARTESIAN_POINT('Ctrl Pts',(101.613182205897,5.73193536297641,336.467258517495));
#19682=CARTESIAN_POINT('Ctrl Pts',(101.620579655101,5.69285872539041,336.619913798193));
#19683=CARTESIAN_POINT('Ctrl Pts',(101.627977104305,5.64766784069477,336.771052526824));
#19684=CARTESIAN_POINT('Ctrl Pts',(101.635374553509,5.5965110391987,336.920154876729));
#19685=CARTESIAN_POINT('Ctrl Pts',(101.642771681973,5.54535645577246,337.069250761817));
#19686=CARTESIAN_POINT('Ctrl Pts',(101.650168810436,5.48823659098824,337.216310090724));
#19687=CARTESIAN_POINT('Ctrl Pts',(101.6575659389,5.42534918934841,337.36082967114));
#19688=CARTESIAN_POINT('Ctrl Pts',(101.664964206336,5.36245210461861,337.505371503964));
#19689=CARTESIAN_POINT('Ctrl Pts',(101.672362473773,5.29378586371869,337.647372467412));
#19690=CARTESIAN_POINT('Ctrl Pts',(101.67976074121,5.21959568977386,337.786350910742));
#19691=CARTESIAN_POINT('Ctrl Pts',(101.687161607735,5.14537945204099,337.92537817866));
#19692=CARTESIAN_POINT('Ctrl Pts',(101.694562474261,5.06563559314468,338.061380483303));
#19693=CARTESIAN_POINT('Ctrl Pts',(101.701963340787,4.9806543801937,338.193902394808));
#19694=CARTESIAN_POINT('Ctrl Pts',(101.709372334171,4.89557984974584,338.326569828041));
#19695=CARTESIAN_POINT('Ctrl Pts',(101.716781327556,4.80525668154069,338.455748921437));
#19696=CARTESIAN_POINT('Ctrl Pts',(101.724190320941,4.71001783857872,338.58101417517));
#19697=CARTESIAN_POINT('Ctrl Pts',(101.731603878521,4.61472032520421,338.706356596621));
#19698=CARTESIAN_POINT('Ctrl Pts',(101.739017436102,4.51450133994696,338.827780086893));
#19699=CARTESIAN_POINT('Ctrl Pts',(101.746430993682,4.40973257147745,338.944894068356));
#19700=CARTESIAN_POINT('Ctrl Pts',(101.753855105819,4.30481464548585,339.062174783012));
#19701=CARTESIAN_POINT('Ctrl Pts',(101.761279217955,4.19533425856126,339.175133468016));
#19702=CARTESIAN_POINT('Ctrl Pts',(101.768703330092,4.08169878720654,339.283417510939));
#19703=CARTESIAN_POINT('Ctrl Pts',(101.772560455246,4.0226605848,339.339675430823));
#19704=CARTESIAN_POINT('Ctrl Pts',(101.776417580401,3.96250136679259,339.394672235018));
#19705=CARTESIAN_POINT('Ctrl Pts',(101.780274705556,3.90128148076729,339.448362998938));
#19706=CARTESIAN_POINT('Ctrl Pts',(101.787698682994,3.78344888929231,339.551703959885));
#19707=CARTESIAN_POINT('Ctrl Pts',(101.795122660432,3.66132961123008,339.650515685064));
#19708=CARTESIAN_POINT('Ctrl Pts',(101.80254663787,3.53530673538617,339.744421655927));
#19709=CARTESIAN_POINT('Ctrl Pts',(101.809961853897,3.409432585497,339.838216803616));
#19710=CARTESIAN_POINT('Ctrl Pts',(101.817377069925,3.27966430415399,339.927117500308));
#19711=CARTESIAN_POINT('Ctrl Pts',(101.824792285952,3.14642037267739,340.010785307804));
#19712=CARTESIAN_POINT('Ctrl Pts',(101.832200367096,3.01330464784049,340.094372610556));
#19713=CARTESIAN_POINT('Ctrl Pts',(101.839608448241,2.8767202446077,340.172736850836));
#19714=CARTESIAN_POINT('Ctrl Pts',(101.847016529385,2.73711705491418,340.245581072693));
#19715=CARTESIAN_POINT('Ctrl Pts',(101.854419096559,2.59761777442511,340.318371075266));
#19716=CARTESIAN_POINT('Ctrl Pts',(101.861821663733,2.45510451091457,340.385649068427));
#19717=CARTESIAN_POINT('Ctrl Pts',(101.869224230907,2.31005425650241,340.447162554442));
#19718=CARTESIAN_POINT('Ctrl Pts',(101.876622900661,2.16508037041392,340.508643653876));
#19719=CARTESIAN_POINT('Ctrl Pts',(101.884021570416,2.01757249630441,340.564366145176));
#19720=CARTESIAN_POINT('Ctrl Pts',(101.891420240171,1.86803013334616,340.614124507295));
#19721=CARTESIAN_POINT('Ctrl Pts',(101.898817689375,1.718512440235,340.66387466083));
#19722=CARTESIAN_POINT('Ctrl Pts',(101.906215138579,1.56696127816549,340.707662520184));
#19723=CARTESIAN_POINT('Ctrl Pts',(101.913612587783,1.41389405050521,340.745331511449));
#19724=CARTESIAN_POINT('Ctrl Pts',(101.921009716246,1.26083345957339,340.782998869451));
#19725=CARTESIAN_POINT('Ctrl Pts',(101.92840684471,1.10625729615029,340.81454779769));
#19726=CARTESIAN_POINT('Ctrl Pts',(101.935803973173,0.950695716283353,340.839872277502));
#19727=CARTESIAN_POINT('Ctrl Pts',(101.94320224061,0.795110183815789,340.865200656652));
#19728=CARTESIAN_POINT('Ctrl Pts',(101.950600508046,0.638539301175376,340.884302619085));
#19729=CARTESIAN_POINT('Ctrl Pts',(101.957998775483,0.481520803051217,340.897123729305));
#19730=CARTESIAN_POINT('Ctrl Pts',(101.965399642009,0.324447142677535,340.909949343715));
#19731=CARTESIAN_POINT('Ctrl Pts',(101.972800508535,0.166925925470569,340.916489682361));
#19732=CARTESIAN_POINT('Ctrl Pts',(101.98020137506,0.00949721230621073,
340.916742377817));
#19733=CARTESIAN_POINT('Ctrl Pts',(101.987610368445,-0.148104372635867,
340.916995350757));
#19734=CARTESIAN_POINT('Ctrl Pts',(101.99501936183,-0.305612877244675,340.910946891384));
#19735=CARTESIAN_POINT('Ctrl Pts',(102.002428355215,-0.462490304256098,
340.89864673302));
#19736=CARTESIAN_POINT('Ctrl Pts',(102.009841912795,-0.619464373174623,
340.886338997334));
#19737=CARTESIAN_POINT('Ctrl Pts',(102.017255470375,-0.77580622008791,340.867771932418));
#19738=CARTESIAN_POINT('Ctrl Pts',(102.024669027955,-0.930986257866573,
340.843046735237));
#19739=CARTESIAN_POINT('Ctrl Pts',(102.032093140092,-1.08638722283786,340.818286337211));
#19740=CARTESIAN_POINT('Ctrl Pts',(102.039517252229,-1.24062271027355,340.787350370209));
#19741=CARTESIAN_POINT('Ctrl Pts',(102.046941364365,-1.39317574605814,340.750390587003));
#19742=CARTESIAN_POINT('Ctrl Pts',(102.05079848952,-1.47243319003586,340.731188491602));
#19743=CARTESIAN_POINT('Ctrl Pts',(102.054655614675,-1.55123678079143,340.710361248204));
#19744=CARTESIAN_POINT('Ctrl Pts',(102.05851273983,-1.6295160827416,340.687935293108));
#19745=CARTESIAN_POINT('Ctrl Pts',(102.065936717268,-1.78018367796471,340.64477107676));
#19746=CARTESIAN_POINT('Ctrl Pts',(102.073360694706,-1.92936231428572,340.595551064847));
#19747=CARTESIAN_POINT('Ctrl Pts',(102.080784672144,-2.07652805789086,340.540393649127));
#19748=CARTESIAN_POINT('Ctrl Pts',(102.088199888171,-2.22352012377637,340.485301327457));
#19749=CARTESIAN_POINT('Ctrl Pts',(102.095615104199,-2.36850367937562,340.424285679292));
#19750=CARTESIAN_POINT('Ctrl Pts',(102.103030320227,-2.51096766053026,340.357515466172));
#19751=CARTESIAN_POINT('Ctrl Pts',(102.110438401371,-2.65329456355895,340.290809499015));
#19752=CARTESIAN_POINT('Ctrl Pts',(102.117846482515,-2.79310638283807,340.218360147391));
#19753=CARTESIAN_POINT('Ctrl Pts',(102.125254563659,-2.92990993943325,340.140385035122));
#19754=CARTESIAN_POINT('Ctrl Pts',(102.132657130833,-3.06661167064293,340.062467961154));
#19755=CARTESIAN_POINT('Ctrl Pts',(102.140059698007,-3.20030927470092,339.979033499991));
#19756=CARTESIAN_POINT('Ctrl Pts',(102.147462265181,-3.33053229306776,339.890346123469));
#19757=CARTESIAN_POINT('Ctrl Pts',(102.154860934935,-3.46068674958587,339.801705440463));
#19758=CARTESIAN_POINT('Ctrl Pts',(102.16225960469,-3.58736995598831,339.70781755958));
#19759=CARTESIAN_POINT('Ctrl Pts',(102.169658274445,-3.7101387775787,339.608991301099));
#19760=CARTESIAN_POINT('Ctrl Pts',(102.177055723649,-3.83288734612491,339.510181345882));
#19761=CARTESIAN_POINT('Ctrl Pts',(102.184453172853,-3.95172252102909,339.406434863739));
#19762=CARTESIAN_POINT('Ctrl Pts',(102.191850622057,-4.06623263929884,339.298102219073));
#19763=CARTESIAN_POINT('Ctrl Pts',(102.19924775052,-4.18073779260942,339.189774271521));
#19764=CARTESIAN_POINT('Ctrl Pts',(102.206644878984,-4.29091799103915,339.076860813308));
#19765=CARTESIAN_POINT('Ctrl Pts',(102.214042007447,-4.39639718337518,338.959750291181));
#19766=CARTESIAN_POINT('Ctrl Pts',(102.221440274884,-4.5018926168741,338.842621736957));
#19767=CARTESIAN_POINT('Ctrl Pts',(102.228838542321,-4.60268535323869,338.721295109394));
#19768=CARTESIAN_POINT('Ctrl Pts',(102.236236809757,-4.69843861740318,338.596193142894));
#19769=CARTESIAN_POINT('Ctrl Pts',(102.243637676283,-4.79422552069579,338.471047226757));
#19770=CARTESIAN_POINT('Ctrl Pts',(102.251038542809,-4.88496920019156,338.342123627166));
#19771=CARTESIAN_POINT('Ctrl Pts',(102.258439409334,-4.97037540714197,338.209875211683));
#19772=CARTESIAN_POINT('Ctrl Pts',(102.265848402719,-5.05587539827319,338.077481574796));
#19773=CARTESIAN_POINT('Ctrl Pts',(102.273257396104,-5.13602600942856,337.941756144546));
#19774=CARTESIAN_POINT('Ctrl Pts',(102.280666389489,-5.21057792122878,337.803178247865));
#19775=CARTESIAN_POINT('Ctrl Pts',(102.288079947069,-5.28517575957793,337.66451498242));
#19776=CARTESIAN_POINT('Ctrl Pts',(102.295493504649,-5.35416786283656,337.52299608374));
#19777=CARTESIAN_POINT('Ctrl Pts',(102.302907062229,-5.41735273970833,337.379121656426));
#19778=CARTESIAN_POINT('Ctrl Pts',(102.310331174366,-5.48062757181996,337.235042397524));
#19779=CARTESIAN_POINT('Ctrl Pts',(102.317755286502,-5.53807852945946,337.088601258819));
#19780=CARTESIAN_POINT('Ctrl Pts',(102.325179398639,-5.5895534604139,336.940315097007));
#19781=CARTESIAN_POINT('Ctrl Pts',(102.329036523794,-5.61629675946009,336.863274465846));
#19782=CARTESIAN_POINT('Ctrl Pts',(102.332893648949,-5.6414278308641,336.785736028709));
#19783=CARTESIAN_POINT('Ctrl Pts',(102.336750774103,-5.66493078873757,336.707773322579));
#19784=CARTESIAN_POINT('Ctrl Pts',(102.345877968528,-5.72054632037482,336.523288570804));
#19785=CARTESIAN_POINT('Ctrl Pts',(102.355005162953,-5.76717819787763,336.335978502897));
#19786=CARTESIAN_POINT('Ctrl Pts',(102.364132357378,-5.8045820679463,336.146628788657));
#19787=CARTESIAN_POINT('Ctrl Pts',(102.373160560046,-5.84158026299218,335.959332724199));
#19788=CARTESIAN_POINT('Ctrl Pts',(102.382188762715,-5.86954951833401,335.770040982889));
#19789=CARTESIAN_POINT('Ctrl Pts',(102.391216965383,-5.88829939689455,335.57953496446));
#19790=CARTESIAN_POINT('Ctrl Pts',(102.400245168051,-5.9070492754551,335.38902894603));
#19791=CARTESIAN_POINT('Ctrl Pts',(102.409273370719,-5.91657961760549,335.197308583576));
#19792=CARTESIAN_POINT('Ctrl Pts',(102.418301573388,-5.91674773493106,335.005177227848));
#19793=CARTESIAN_POINT('',(104.168301675714,-5.91240382638103,334.997402536992));
#19794=CARTESIAN_POINT('Ctrl Pts',(102.418301620294,-5.91325220417344,335.005173171578));
#19795=CARTESIAN_POINT('Ctrl Pts',(102.483864016322,-5.9016191688865,333.610737067852));
#19796=CARTESIAN_POINT('Ctrl Pts',(102.642172423775,-4.71167084592652,330.225837329939));
#19797=CARTESIAN_POINT('Ctrl Pts',(102.893226842651,0.937317003455184,328.066454027249));
#19798=CARTESIAN_POINT('Ctrl Pts',(103.171464876926,6.3378027430104,332.036070292348));
#19799=CARTESIAN_POINT('Ctrl Pts',(103.4497029112,5.92218045112015,338.725641102628));
#19800=CARTESIAN_POINT('Ctrl Pts',(103.727940945472,0.0718605704745667,
341.996246063401));
#19801=CARTESIAN_POINT('Ctrl Pts',(103.967473848504,-5.02140497767314,339.284654193084));
#19802=CARTESIAN_POINT('Ctrl Pts',(104.114260740112,-5.90351638125909,336.149335155669));
#19803=CARTESIAN_POINT('Ctrl Pts',(104.168301620294,-5.90805822426525,334.99740562831));
#19804=CARTESIAN_POINT('',(105.918301620294,-5.91976240380336,334.995907611496));
#19805=CARTESIAN_POINT('Ctrl Pts',(104.168301675755,-5.91674942901628,334.997400627864));
#19806=CARTESIAN_POINT('Ctrl Pts',(104.176377585023,-5.91667369032755,334.825002517902));
#19807=CARTESIAN_POINT('Ctrl Pts',(104.184453494291,-5.90905900258697,334.652848612642));
#19808=CARTESIAN_POINT('Ctrl Pts',(104.192529403559,-5.89399401348954,334.481574372306));
#19809=CARTESIAN_POINT('Ctrl Pts',(104.200642131212,-5.87886034252009,334.309519286039));
#19810=CARTESIAN_POINT('Ctrl Pts',(104.208754858865,-5.85620836299364,334.138352149417));
#19811=CARTESIAN_POINT('Ctrl Pts',(104.216867586518,-5.82617848403943,333.968702354014));
#19812=CARTESIAN_POINT('Ctrl Pts',(104.224998802207,-5.79608017021225,333.798665944925));
#19813=CARTESIAN_POINT('Ctrl Pts',(104.233130017896,-5.75857040477857,333.630154032497));
#19814=CARTESIAN_POINT('Ctrl Pts',(104.241261233585,-5.71383973478456,333.463781900999));
#19815=CARTESIAN_POINT('Ctrl Pts',(104.249420485457,-5.66895483481357,333.2968361235));
#19816=CARTESIAN_POINT('Ctrl Pts',(104.257579737328,-5.61679926657378,333.132045135939));
#19817=CARTESIAN_POINT('Ctrl Pts',(104.265738989199,-5.5576132958972,332.970008616825));
#19818=CARTESIAN_POINT('Ctrl Pts',(104.271964997473,-5.51245077990218,332.846364841067));
#19819=CARTESIAN_POINT('Ctrl Pts',(104.278191005748,-5.46319571390982,332.724324464125));
#19820=CARTESIAN_POINT('Ctrl Pts',(104.284417014022,-5.40997276369408,332.604144149038));
#19821=CARTESIAN_POINT('Ctrl Pts',(104.29184099146,-5.34650898976519,332.460839497258));
#19822=CARTESIAN_POINT('Ctrl Pts',(104.299264968898,-5.27725155469762,332.319842040562));
#19823=CARTESIAN_POINT('Ctrl Pts',(104.306688946336,-5.20238974119466,332.18165446703));
#19824=CARTESIAN_POINT('Ctrl Pts',(104.314104162363,-5.1276162758952,332.043629975626));
#19825=CARTESIAN_POINT('Ctrl Pts',(104.321519378391,-5.04725177349629,331.908409091629));
#19826=CARTESIAN_POINT('Ctrl Pts',(104.328934594418,-4.96153363947666,331.776474832293));
#19827=CARTESIAN_POINT('Ctrl Pts',(104.336342675563,-4.87589798301393,331.644667519437));
#19828=CARTESIAN_POINT('Ctrl Pts',(104.343750756707,-4.78491915205543,331.516140846414));
#19829=CARTESIAN_POINT('Ctrl Pts',(104.351158837851,-4.68888049227543,331.391353398896));
#19830=CARTESIAN_POINT('Ctrl Pts',(104.358561405025,-4.59291331582377,331.266658832954));
#19831=CARTESIAN_POINT('Ctrl Pts',(104.365963972199,-4.49189403609786,331.145698245306));
#19832=CARTESIAN_POINT('Ctrl Pts',(104.373366539373,-4.38614927922281,331.028901277622));
#19833=CARTESIAN_POINT('Ctrl Pts',(104.380765209127,-4.2804601965004,330.912165803031));
#19834=CARTESIAN_POINT('Ctrl Pts',(104.388163878882,-4.17005084136955,330.799589858619));
#19835=CARTESIAN_POINT('Ctrl Pts',(104.395562548637,-4.05528801181642,330.691569925864));
#19836=CARTESIAN_POINT('Ctrl Pts',(104.40295999784,-3.94054411456643,330.583567813043));
#19837=CARTESIAN_POINT('Ctrl Pts',(104.410357447044,-3.82144843976441,330.480120475742));
#19838=CARTESIAN_POINT('Ctrl Pts',(104.417754896248,-3.69840460943225,330.381587512204));
#19839=CARTESIAN_POINT('Ctrl Pts',(104.425152024712,-3.57536611406615,330.283058820884));
#19840=CARTESIAN_POINT('Ctrl Pts',(104.432549153175,-3.44838009485832,330.189444312941));
#19841=CARTESIAN_POINT('Ctrl Pts',(104.439946281638,-3.31788299989221,330.10106307843));
#19842=CARTESIAN_POINT('Ctrl Pts',(104.447344549075,-3.18736581163103,330.012668235414));
#19843=CARTESIAN_POINT('Ctrl Pts',(104.454742816511,-3.05333678019932,329.929508479565));
#19844=CARTESIAN_POINT('Ctrl Pts',(104.462141083948,-2.91626091739829,329.851859284736));
#19845=CARTESIAN_POINT('Ctrl Pts',(104.469541950474,-2.77913689840513,329.774182810929));
#19846=CARTESIAN_POINT('Ctrl Pts',(104.476942816999,-2.6389642414352,329.702020936384));
#19847=CARTESIAN_POINT('Ctrl Pts',(104.484343683525,-2.49623196021103,329.635602870469));
#19848=CARTESIAN_POINT('Ctrl Pts',(104.49175267691,-2.35334294529623,329.569111871167));
#19849=CARTESIAN_POINT('Ctrl Pts',(104.499161670294,-2.20788903155726,329.508377433961));
#19850=CARTESIAN_POINT('Ctrl Pts',(104.506570663679,-2.06037926541668,329.453580628447));
#19851=CARTESIAN_POINT('Ctrl Pts',(104.513984221259,-1.912778628172,329.39875006621));
#19852=CARTESIAN_POINT('Ctrl Pts',(104.521397778839,-1.76311996884052,329.3498645399));
#19853=CARTESIAN_POINT('Ctrl Pts',(104.528811336419,-1.61192634034383,329.307054889093));
#19854=CARTESIAN_POINT('Ctrl Pts',(104.536235448556,-1.46051746003739,329.264184290909));
#19855=CARTESIAN_POINT('Ctrl Pts',(104.543659560693,-1.30756960795487,329.22740693127));
#19856=CARTESIAN_POINT('Ctrl Pts',(104.551083672829,-1.15361564846502,329.196802476383));
#19857=CARTESIAN_POINT('Ctrl Pts',(104.554940797984,-1.07363036821326,329.180902229912));
#19858=CARTESIAN_POINT('Ctrl Pts',(104.558797923139,-0.993373607276174,
329.166667332352));
#19859=CARTESIAN_POINT('Ctrl Pts',(104.562655048294,-0.912920388189857,
329.154103411167));
#19860=CARTESIAN_POINT('Ctrl Pts',(104.570079025732,-0.758068559613185,
329.129921082707));
#19861=CARTESIAN_POINT('Ctrl Pts',(104.57750300317,-0.602021618121262,329.111859323147));
#19862=CARTESIAN_POINT('Ctrl Pts',(104.584926980608,-0.445304716578557,
329.100030993989));
#19863=CARTESIAN_POINT('Ctrl Pts',(104.592342196636,-0.288772764559113,
329.088216624039));
#19864=CARTESIAN_POINT('Ctrl Pts',(104.599757412663,-0.131572794831305,
329.082621069304));
#19865=CARTESIAN_POINT('Ctrl Pts',(104.607172628691,0.0257605393623651,
329.083306078805));
#19866=CARTESIAN_POINT('Ctrl Pts',(104.614580709835,0.182942488214167,329.083990429193));
#19867=CARTESIAN_POINT('Ctrl Pts',(104.621988790979,0.340257175351975,329.090943311462));
#19868=CARTESIAN_POINT('Ctrl Pts',(104.629396872123,0.497165631698212,329.104174621212));
#19869=CARTESIAN_POINT('Ctrl Pts',(104.636799439297,0.653957298214561,329.117396082657));
#19870=CARTESIAN_POINT('Ctrl Pts',(104.644202006471,0.810342965693608,329.136886635437));
#19871=CARTESIAN_POINT('Ctrl Pts',(104.651604573645,0.965784583151705,329.162604116436));
#19872=CARTESIAN_POINT('Ctrl Pts',(104.6590032434,1.12114436127767,329.188308057294));
#19873=CARTESIAN_POINT('Ctrl Pts',(104.666401913155,1.27556071198526,329.220232336377));
#19874=CARTESIAN_POINT('Ctrl Pts',(104.67380058291,1.42850173010513,329.25828306431));
#19875=CARTESIAN_POINT('Ctrl Pts',(104.681198032114,1.58141751770619,329.296327515055));
#19876=CARTESIAN_POINT('Ctrl Pts',(104.688595481318,1.73285809393971,329.34049631877));
#19877=CARTESIAN_POINT('Ctrl Pts',(104.695992930522,1.8823026419341,329.390644660331));
#19878=CARTESIAN_POINT('Ctrl Pts',(104.703390058985,2.03174071027321,329.440790827548));
#19879=CARTESIAN_POINT('Ctrl Pts',(104.710787187449,2.17918256863004,329.496915898381));
#19880=CARTESIAN_POINT('Ctrl Pts',(104.718184315912,2.3241237002702,329.558825532264));
#19881=CARTESIAN_POINT('Ctrl Pts',(104.725582583349,2.46908714922652,329.620744698685));
#19882=CARTESIAN_POINT('Ctrl Pts',(104.732980850786,2.61154876154769,329.688450055005));
#19883=CARTESIAN_POINT('Ctrl Pts',(104.740379118222,2.75102524082544,329.761699637588));
#19884=CARTESIAN_POINT('Ctrl Pts',(104.747779984748,2.89055071965723,329.834974953521));
#19885=CARTESIAN_POINT('Ctrl Pts',(104.755180851274,3.02708864726,329.913798200257));
#19886=CARTESIAN_POINT('Ctrl Pts',(104.7625817178,3.16018164320287,329.997882194064));
#19887=CARTESIAN_POINT('Ctrl Pts',(104.769990711184,3.29342078797948,330.082058520135));
#19888=CARTESIAN_POINT('Ctrl Pts',(104.777399704569,3.42320713080698,330.171506930408));
#19889=CARTESIAN_POINT('Ctrl Pts',(104.784808697954,3.54911293216977,330.265897344036));
#19890=CARTESIAN_POINT('Ctrl Pts',(104.792222255534,3.67509629584916,330.360345905414));
#19891=CARTESIAN_POINT('Ctrl Pts',(104.799635813114,3.79719406582669,330.459742301537));
#19892=CARTESIAN_POINT('Ctrl Pts',(104.807049370695,3.91501316236303,330.563717490846));
#19893=CARTESIAN_POINT('Ctrl Pts',(104.814473482831,4.03299999595296,330.667840707872));
#19894=CARTESIAN_POINT('Ctrl Pts',(104.821897594968,4.14669572119251,330.776555480103));
#19895=CARTESIAN_POINT('Ctrl Pts',(104.829321707105,4.25574498158056,330.889456822481));
#19896=CARTESIAN_POINT('Ctrl Pts',(104.83317883226,4.31240046274745,330.948113615328));
#19897=CARTESIAN_POINT('Ctrl Pts',(104.837035957414,4.36780243026257,331.007899917929));
#19898=CARTESIAN_POINT('Ctrl Pts',(104.840893082569,4.42190555287358,331.068755687576));
#19899=CARTESIAN_POINT('Ctrl Pts',(104.848317060007,4.52604019862202,331.185887448333));
#19900=CARTESIAN_POINT('Ctrl Pts',(104.855741037445,4.62567467157974,331.307336396068));
#19901=CARTESIAN_POINT('Ctrl Pts',(104.863165014883,4.72042987375358,331.432721994367));
#19902=CARTESIAN_POINT('Ctrl Pts',(104.870580230911,4.81507325053216,331.557959618794));
#19903=CARTESIAN_POINT('Ctrl Pts',(104.877995446938,4.90484859563693,331.687124351313));
#19904=CARTESIAN_POINT('Ctrl Pts',(104.885410662966,4.98941465145081,331.819800006542));
#19905=CARTESIAN_POINT('Ctrl Pts',(104.89281874411,5.07389933823157,331.952348001924));
#19906=CARTESIAN_POINT('Ctrl Pts',(104.900226825254,5.1531845151227,332.088399882053));
#19907=CARTESIAN_POINT('Ctrl Pts',(104.907634906398,5.22697019361061,332.227507771407));
#19908=CARTESIAN_POINT('Ctrl Pts',(104.915037473572,5.30070095207048,332.36651212022));
#19909=CARTESIAN_POINT('Ctrl Pts',(104.922440040746,5.36894018850547,332.508567620822));
#19910=CARTESIAN_POINT('Ctrl Pts',(104.92984260792,5.43143218851948,332.653198997781));
#19911=CARTESIAN_POINT('Ctrl Pts',(104.937241277675,5.4938912867686,332.797754226953));
#19912=CARTESIAN_POINT('Ctrl Pts',(104.94463994743,5.55060902718935,332.944882289818));
#19913=CARTESIAN_POINT('Ctrl Pts',(104.952038617184,5.60137651895223,333.094085087043));
#19914=CARTESIAN_POINT('Ctrl Pts',(104.959436066388,5.65213563565539,333.24326327044));
#19915=CARTESIAN_POINT('Ctrl Pts',(104.966833515592,5.69694633176932,333.394515155934));
#19916=CARTESIAN_POINT('Ctrl Pts',(104.974230964796,5.73564854152856,333.547324409732));
#19917=CARTESIAN_POINT('Ctrl Pts',(104.98162809326,5.77434907322746,333.700127037987));
#19918=CARTESIAN_POINT('Ctrl Pts',(104.989025221723,5.80694155355679,333.854486538497));
#19919=CARTESIAN_POINT('Ctrl Pts',(104.996422350187,5.83331638469168,334.009873483545));
#19920=CARTESIAN_POINT('Ctrl Pts',(105.003820617623,5.85969527689218,334.165284354303));
#19921=CARTESIAN_POINT('Ctrl Pts',(105.01121888506,5.87985455120487,334.321722616627));
#19922=CARTESIAN_POINT('Ctrl Pts',(105.018617152496,5.89373614059483,334.478650915848));
#19923=CARTESIAN_POINT('Ctrl Pts',(105.026018019022,5.90762260673312,334.635634345631));
#19924=CARTESIAN_POINT('Ctrl Pts',(105.033418885548,5.91522696410329,334.793107783546));
#19925=CARTESIAN_POINT('Ctrl Pts',(105.040819752074,5.9165431968366,334.950531197037));
#19926=CARTESIAN_POINT('Ctrl Pts',(105.048228745458,5.91786087491929,335.108127476486));
#19927=CARTESIAN_POINT('Ctrl Pts',(105.055637738843,5.91287663566499,335.265673248387));
#19928=CARTESIAN_POINT('Ctrl Pts',(105.063046732228,5.90163657670515,335.42263019177));
#19929=CARTESIAN_POINT('Ctrl Pts',(105.070460289808,5.89038959348128,335.579683826045));
#19930=CARTESIAN_POINT('Ctrl Pts',(105.077873847388,5.87287915275581,335.736147538967));
#19931=CARTESIAN_POINT('Ctrl Pts',(105.085287404969,5.8492028714466,335.891491071835));
#19932=CARTESIAN_POINT('Ctrl Pts',(105.092711517105,5.82549288261645,336.047055764661));
#19933=CARTESIAN_POINT('Ctrl Pts',(105.100135629242,5.79559959210596,336.201496726913));
#19934=CARTESIAN_POINT('Ctrl Pts',(105.107559741379,5.75967125669765,336.354295971075));
#19935=CARTESIAN_POINT('Ctrl Pts',(105.111416866533,5.74100503995453,336.433681330216));
#19936=CARTESIAN_POINT('Ctrl Pts',(105.115273991688,5.72071064619899,336.512623825523));
#19937=CARTESIAN_POINT('Ctrl Pts',(105.119131116843,5.69881403528363,336.591052844425));
#19938=CARTESIAN_POINT('Ctrl Pts',(105.126555094281,5.65666867082547,336.742008606415));
#19939=CARTESIAN_POINT('Ctrl Pts',(105.133979071719,5.60845759001825,336.891516354692));
#19940=CARTESIAN_POINT('Ctrl Pts',(105.141403049157,5.55429564237294,337.039051367577));
#19941=CARTESIAN_POINT('Ctrl Pts',(105.148818265184,5.50019761397491,337.186412266949));
#19942=CARTESIAN_POINT('Ctrl Pts',(105.156233481212,5.44016282533593,337.331804718157));
#19943=CARTESIAN_POINT('Ctrl Pts',(105.163648697239,5.37435658154257,337.474716528601));
#19944=CARTESIAN_POINT('Ctrl Pts',(105.171056778384,5.30861365618565,337.61749083002));
#19945=CARTESIAN_POINT('Ctrl Pts',(105.178464859528,5.23711048624453,337.757788905736));
#19946=CARTESIAN_POINT('Ctrl Pts',(105.185872940672,5.16006135880073,337.895116117863));
#19947=CARTESIAN_POINT('Ctrl Pts',(105.193275507846,5.08306958042967,338.032341114839));
#19948=CARTESIAN_POINT('Ctrl Pts',(105.20067807502,5.00054024575367,338.166599327096));
#19949=CARTESIAN_POINT('Ctrl Pts',(105.208080642194,4.91273464229113,338.297418520136));
#19950=CARTESIAN_POINT('Ctrl Pts',(105.215479311948,4.82497526809506,338.428168837442));
#19951=CARTESIAN_POINT('Ctrl Pts',(105.222877981703,4.73194536499745,338.555483432404));
#19952=CARTESIAN_POINT('Ctrl Pts',(105.230276651458,4.63395075253962,338.678917094138));
#19953=CARTESIAN_POINT('Ctrl Pts',(105.237674100662,4.53597230614996,338.80233039315));
#19954=CARTESIAN_POINT('Ctrl Pts',(105.245071549866,4.43303100772558,338.921863737578));
#19955=CARTESIAN_POINT('Ctrl Pts',(105.25246899907,4.32547443259754,339.037103106863));
#19956=CARTESIAN_POINT('Ctrl Pts',(105.259866127533,4.21792252093509,339.15233747957));
#19957=CARTESIAN_POINT('Ctrl Pts',(105.267263255997,4.10575598510295,339.263277974482));
#19958=CARTESIAN_POINT('Ctrl Pts',(105.27466038446,3.98936072249202,339.369545924732));
#19959=CARTESIAN_POINT('Ctrl Pts',(105.282058651897,3.87294753791625,339.475830237593));
#19960=CARTESIAN_POINT('Ctrl Pts',(105.289456919334,3.75230460573427,339.57744032161));
#19961=CARTESIAN_POINT('Ctrl Pts',(105.29685518677,3.62785237554537,339.674036553532));
#19962=CARTESIAN_POINT('Ctrl Pts',(105.304256053296,3.50335642397915,339.770666720725));
#19963=CARTESIAN_POINT('Ctrl Pts',(105.311656919822,3.37504880459844,339.86227930015));
#19964=CARTESIAN_POINT('Ctrl Pts',(105.319057786347,3.2433803867706,339.948576990329));
#19965=CARTESIAN_POINT('Ctrl Pts',(105.326466779732,3.11156738443189,340.034969443622));
#19966=CARTESIAN_POINT('Ctrl Pts',(105.333875773117,2.97638652589233,340.11603514765));
#19967=CARTESIAN_POINT('Ctrl Pts',(105.341284766502,2.83831544281442,340.191521550526));
#19968=CARTESIAN_POINT('Ctrl Pts',(105.348698324082,2.70015930318685,340.267054455631));
#19969=CARTESIAN_POINT('Ctrl Pts',(105.356111881662,2.5591097247587,340.337001045404));
#19970=CARTESIAN_POINT('Ctrl Pts',(105.363525439242,2.41566543950032,340.401156454585));
#19971=CARTESIAN_POINT('Ctrl Pts',(105.370949551379,2.27201693504089,340.465403200736));
#19972=CARTESIAN_POINT('Ctrl Pts',(105.378373663516,2.12596726025782,340.523842161495));
#19973=CARTESIAN_POINT('Ctrl Pts',(105.385797775653,1.97803223215624,340.576317696388));
#19974=CARTESIAN_POINT('Ctrl Pts',(105.389654900807,1.90117402909435,340.603580849465));
#19975=CARTESIAN_POINT('Ctrl Pts',(105.393512025962,1.82380713967182,340.629235174725));
#19976=CARTESIAN_POINT('Ctrl Pts',(105.397369151117,1.74600499187263,340.653264289847));
#19977=CARTESIAN_POINT('Ctrl Pts',(105.404793128555,1.59625579610632,340.699514178395));
#19978=CARTESIAN_POINT('Ctrl Pts',(105.412217105993,1.44444175879629,340.739879673351));
#19979=CARTESIAN_POINT('Ctrl Pts',(105.419641083431,1.29106628125662,340.774173397111));
#19980=CARTESIAN_POINT('Ctrl Pts',(105.427056299458,1.13787180985702,340.808426649117));
#19981=CARTESIAN_POINT('Ctrl Pts',(105.434471515486,0.983119926896012,340.83662231253));
#19982=CARTESIAN_POINT('Ctrl Pts',(105.441886731514,0.827330802125772,340.858622219119));
#19983=CARTESIAN_POINT('Ctrl Pts',(105.449294812658,0.67169157686698,340.880600957508));
#19984=CARTESIAN_POINT('Ctrl Pts',(105.456702893802,0.515017463763272,340.896395755523));
#19985=CARTESIAN_POINT('Ctrl Pts',(105.464110974946,0.357840377399421,340.905919134801));
#19986=CARTESIAN_POINT('Ctrl Pts',(105.47151354212,0.20078028081135,340.915435425653));
#19987=CARTESIAN_POINT('Ctrl Pts',(105.478916109294,0.0432183273251074,
340.918689569825));
#19988=CARTESIAN_POINT('Ctrl Pts',(105.486318676468,-0.11430697332543,340.91564573638));
#19989=CARTESIAN_POINT('Ctrl Pts',(105.493717346223,-0.271749337593634,
340.9126035055));
#19990=CARTESIAN_POINT('Ctrl Pts',(105.501116015978,-0.429154715256507,
340.903269907923));
#19991=CARTESIAN_POINT('Ctrl Pts',(105.508514685732,-0.585983222481062,
340.88766118467));
#19992=CARTESIAN_POINT('Ctrl Pts',(105.515912134936,-0.74278585787171,340.872055036372));
#19993=CARTESIAN_POINT('Ctrl Pts',(105.52330958414,-0.899011440681882,340.850175853862));
#19994=CARTESIAN_POINT('Ctrl Pts',(105.530707033344,-1.0541237192351,340.822091870371));
#19995=CARTESIAN_POINT('Ctrl Pts',(105.538104161808,-1.20922927239024,340.794009104554));
#19996=CARTESIAN_POINT('Ctrl Pts',(105.545501290271,-1.3632212500264,340.759722139165));
#19997=CARTESIAN_POINT('Ctrl Pts',(105.552898418735,-1.51557239187673,340.719350565185));
#19998=CARTESIAN_POINT('Ctrl Pts',(105.560296686171,-1.66794699199993,340.67897277499));
#19999=CARTESIAN_POINT('Ctrl Pts',(105.567694953608,-1.8186798925005,340.632508606361));
#20000=CARTESIAN_POINT('Ctrl Pts',(105.575093221045,-1.96725796753637,340.580127834706));
#20001=CARTESIAN_POINT('Ctrl Pts',(105.58249408757,-2.11588823961227,340.527728661135));
#20002=CARTESIAN_POINT('Ctrl Pts',(105.589894954096,-2.2623618272558,340.46940887013));
#20003=CARTESIAN_POINT('Ctrl Pts',(105.597295820622,-2.4061847320271,340.405386720472));
#20004=CARTESIAN_POINT('Ctrl Pts',(105.604704814007,-2.55016556809806,340.341294268373));
#20005=CARTESIAN_POINT('Ctrl Pts',(105.612113807391,-2.69148956730769,340.271487104468));
#20006=CARTESIAN_POINT('Ctrl Pts',(105.619522800776,-2.82968587948925,340.196230209096));
#20007=CARTESIAN_POINT('Ctrl Pts',(105.626936358356,-2.96796732536612,340.12092695288));
#20008=CARTESIAN_POINT('Ctrl Pts',(105.634349915937,-3.10311692526235,340.040167466479));
#20009=CARTESIAN_POINT('Ctrl Pts',(105.641763473517,-3.234692511123,339.954260279899));
#20010=CARTESIAN_POINT('Ctrl Pts',(105.649187585654,-3.36645541891807,339.868230788712));
#20011=CARTESIAN_POINT('Ctrl Pts',(105.65661169779,-3.49463384711528,339.777039176247));
#20012=CARTESIAN_POINT('Ctrl Pts',(105.664035809927,-3.61881777613905,339.681034978036));
#20013=CARTESIAN_POINT('Ctrl Pts',(105.667892935081,-3.68333632699171,339.631156931875));
#20014=CARTESIAN_POINT('Ctrl Pts',(105.671750060236,-3.74677725958832,339.579980491455));
#20015=CARTESIAN_POINT('Ctrl Pts',(105.675607185391,-3.80908706159064,339.52755853852));
#20016=CARTESIAN_POINT('Ctrl Pts',(105.682926719848,-3.92733024129565,339.428079191736));
#20017=CARTESIAN_POINT('Ctrl Pts',(105.690246254305,-4.04187637728178,339.323793849167));
#20018=CARTESIAN_POINT('Ctrl Pts',(105.697565788763,-4.15230161964887,339.215011485389));
#20019=CARTESIAN_POINT('Ctrl Pts',(105.704876630412,-4.26259571905414,339.106358313462));
#20020=CARTESIAN_POINT('Ctrl Pts',(105.712187472062,-4.36877839062624,338.993219013035));
#20021=CARTESIAN_POINT('Ctrl Pts',(105.719498313711,-4.47045756742951,338.875943717382));
#20022=CARTESIAN_POINT('Ctrl Pts',(105.726802174549,-4.57203965511264,338.758780402919));
#20023=CARTESIAN_POINT('Ctrl Pts',(105.734106035387,-4.66912655475497,338.63748924053));
#20024=CARTESIAN_POINT('Ctrl Pts',(105.741409896225,-4.76136210197062,338.512458041944));
#20025=CARTESIAN_POINT('Ctrl Pts',(105.748780384728,-4.85443904516614,338.386286277155));
#20026=CARTESIAN_POINT('Ctrl Pts',(105.756150873231,-4.94257538854965,338.256306165677));
#20027=CARTESIAN_POINT('Ctrl Pts',(105.763521361733,-5.02544536141048,338.122952046058));
#20028=CARTESIAN_POINT('Ctrl Pts',(105.77081673526,-5.10747078020508,337.990956980389));
#20029=CARTESIAN_POINT('Ctrl Pts',(105.778112108787,-5.1843364660858,337.855656693525));
#20030=CARTESIAN_POINT('Ctrl Pts',(105.785407482314,-5.25576921250541,337.717502630611));
#20031=CARTESIAN_POINT('Ctrl Pts',(105.792701419185,-5.32718789189067,337.579375773959));
#20032=CARTESIAN_POINT('Ctrl Pts',(105.799995356055,-5.39317558391413,337.438396600875));
#20033=CARTESIAN_POINT('Ctrl Pts',(105.807289292926,-5.45350483718485,337.295041514505));
#20034=CARTESIAN_POINT('Ctrl Pts',(105.81458332757,-5.51383489914462,337.151684506518));
#20035=CARTESIAN_POINT('Ctrl Pts',(105.821877362213,-5.56850622303597,337.005951876731));
#20036=CARTESIAN_POINT('Ctrl Pts',(105.829171396856,-5.61733946573983,336.858340089742));
#20037=CARTESIAN_POINT('Ctrl Pts',(105.836598915476,-5.66706637782536,336.708026943451));
#20038=CARTESIAN_POINT('Ctrl Pts',(105.844026434096,-5.71073930474988,336.555765579812));
#20039=CARTESIAN_POINT('Ctrl Pts',(105.851453952715,-5.74822216767177,336.402095743374));
#20040=CARTESIAN_POINT('Ctrl Pts',(105.858755885835,-5.78507126522119,336.251024177546));
#20041=CARTESIAN_POINT('Ctrl Pts',(105.866057818954,-5.81593794289666,336.098591782589));
#20042=CARTESIAN_POINT('Ctrl Pts',(105.873359752073,-5.84074480762381,335.945320397916));
#20043=CARTESIAN_POINT('Ctrl Pts',(105.880850063443,-5.86619164997221,335.788094855502));
#20044=CARTESIAN_POINT('Ctrl Pts',(105.888340374813,-5.88526172827391,335.629986881795));
#20045=CARTESIAN_POINT('Ctrl Pts',(105.895830686184,-5.89792834386354,335.471563159239));
#20046=CARTESIAN_POINT('Ctrl Pts',(105.903320997554,-5.91059495945317,335.313139436682));
#20047=CARTESIAN_POINT('Ctrl Pts',(105.910811308924,-5.91685815230932,335.154400398292));
#20048=CARTESIAN_POINT('Ctrl Pts',(105.918301620294,-5.91674858616663,334.995909694977));
#20049=CARTESIAN_POINT('',(107.668301620294,-5.92094148725317,335.004780648189));
#20050=CARTESIAN_POINT('Ctrl Pts',(105.918301620294,-5.92277622144009,334.995905528015));
#20051=CARTESIAN_POINT('Ctrl Pts',(105.930149486751,-5.92475648142696,334.744954570789));
#20052=CARTESIAN_POINT('Ctrl Pts',(106.034743364634,-5.79618199096297,332.531584302122));
#20053=CARTESIAN_POINT('Ctrl Pts',(106.232083253937,-3.00667844047728,328.682365341618));
#20054=CARTESIAN_POINT('Ctrl Pts',(106.510321288213,3.68554753774321,329.052785335281));
#20055=CARTESIAN_POINT('Ctrl Pts',(106.788559322486,6.99560093916926,334.880876446012));
#20056=CARTESIAN_POINT('Ctrl Pts',(107.066797356761,3.88589461361887,340.818285483979));
#20057=CARTESIAN_POINT('Ctrl Pts',(107.345035391035,-2.78983984313537,341.416339811048));
#20058=CARTESIAN_POINT('Ctrl Pts',(107.545536812213,-5.75554344655869,337.60421618645));
#20059=CARTESIAN_POINT('Ctrl Pts',(107.653292221966,-5.92373472965658,335.322952874196));
#20060=CARTESIAN_POINT('Ctrl Pts',(107.668301620294,-5.92094148725317,335.004780648189));
#20061=CARTESIAN_POINT('',(109.418301620294,-5.9073481418614,335.001565332871));
#20062=CARTESIAN_POINT('Ctrl Pts',(107.668301620294,-5.92094148725317,335.004780648189));
#20063=CARTESIAN_POINT('Ctrl Pts',(107.74603823339,-5.90647473787108,333.356904384973));
#20064=CARTESIAN_POINT('Ctrl Pts',(107.916520857911,-4.33224609725952,329.718746258985));
#20065=CARTESIAN_POINT('Ctrl Pts',(108.179749493857,1.83586661996066,328.248539663529));
#20066=CARTESIAN_POINT('Ctrl Pts',(108.457987528129,6.67093980309293,332.890216820446));
#20067=CARTESIAN_POINT('Ctrl Pts',(108.736225562404,5.38418999183579,339.468010860891));
#20068=CARTESIAN_POINT('Ctrl Pts',(109.014463596677,-0.84355150441294,341.945577282027));
#20069=CARTESIAN_POINT('Ctrl Pts',(109.241822282641,-5.29991352060222,338.761775431531));
#20070=CARTESIAN_POINT('Ctrl Pts',(109.37643495718,-5.90945668690147,335.894258462759));
#20071=CARTESIAN_POINT('Ctrl Pts',(109.418301620294,-5.9073481418614,335.001565332871));
#20072=CARTESIAN_POINT('',(111.168301624698,-5.91548968584153,334.994581587743));
#20073=CARTESIAN_POINT('Ctrl Pts',(109.418301620294,-5.9073481418614,335.001565332871));
#20074=CARTESIAN_POINT('Ctrl Pts',(109.469180968605,-5.9047856878815,333.916701116055));
#20075=CARTESIAN_POINT('Ctrl Pts',(109.612806328339,-5.09840548129149,330.850735185492));
#20076=CARTESIAN_POINT('Ctrl Pts',(109.8491776995,-0.166381100682085,328.005363465443));
#20077=CARTESIAN_POINT('Ctrl Pts',(110.127415733773,5.79190072541038,331.074887401844));
#20078=CARTESIAN_POINT('Ctrl Pts',(110.405653768048,6.43504074410829,337.746429235006));
#20079=CARTESIAN_POINT('Ctrl Pts',(110.683891802322,1.17283885298437,341.89761349643));
#20080=CARTESIAN_POINT('Ctrl Pts',(110.938107753071,-4.61841647199816,339.907056893972));
#20081=CARTESIAN_POINT('Ctrl Pts',(111.099577692395,-5.90208330670883,336.455049090138));
#20082=CARTESIAN_POINT('Ctrl Pts',(111.168301620294,-5.91518394046082,334.994581961406));
#20083=CARTESIAN_POINT('',(112.91830226473,-5.92197236043631,335.001102995849));
#20084=CARTESIAN_POINT('Ctrl Pts',(111.168301642816,-5.91674751756803,334.994580050503));
#20085=CARTESIAN_POINT('Ctrl Pts',(111.177681833011,-5.91656486805913,334.79518870395));
#20086=CARTESIAN_POINT('Ctrl Pts',(111.187062023205,-5.90629965081535,334.596247156779));
#20087=CARTESIAN_POINT('Ctrl Pts',(111.1964422134,-5.88610916826479,334.398627052679));
#20088=CARTESIAN_POINT('Ctrl Pts',(111.206007905427,-5.86551940047264,334.197098830444));
#20089=CARTESIAN_POINT('Ctrl Pts',(111.215573597454,-5.83460793238311,333.996944643371));
#20090=CARTESIAN_POINT('Ctrl Pts',(111.225139289481,-5.79358985553926,333.79906405321));
#20091=CARTESIAN_POINT('Ctrl Pts',(111.230215483277,-5.77182292988356,333.694055422232));
#20092=CARTESIAN_POINT('Ctrl Pts',(111.235291677073,-5.74721071566286,333.589686654878));
#20093=CARTESIAN_POINT('Ctrl Pts',(111.240367870869,-5.71979075055661,333.48608972117));
#20094=CARTESIAN_POINT('Ctrl Pts',(111.247791848307,-5.67968881385373,333.334578307422));
#20095=CARTESIAN_POINT('Ctrl Pts',(111.255215825745,-5.63350215019534,333.184432820619));
#20096=CARTESIAN_POINT('Ctrl Pts',(111.262639803183,-5.58133850903378,333.036179486288));
#20097=CARTESIAN_POINT('Ctrl Pts',(111.270055019211,-5.5292364288172,332.888101113197));
#20098=CARTESIAN_POINT('Ctrl Pts',(111.277470235238,-5.47117153433217,332.741910796337));
#20099=CARTESIAN_POINT('Ctrl Pts',(111.284885451266,-5.40730219528288,332.598122915012));
#20100=CARTESIAN_POINT('Ctrl Pts',(111.29229353241,-5.34349431099007,332.454473385663));
#20101=CARTESIAN_POINT('Ctrl Pts',(111.299701613554,-5.2738932513323,332.313222028659));
#20102=CARTESIAN_POINT('Ctrl Pts',(111.307109694698,-5.19870660072143,332.174866331991));
#20103=CARTESIAN_POINT('Ctrl Pts',(111.314512261872,-5.12357591290791,332.036613615996));
#20104=CARTESIAN_POINT('Ctrl Pts',(111.321914829046,-5.04286808968227,331.901252595349));
#20105=CARTESIAN_POINT('Ctrl Pts',(111.32931739622,-4.95683801429786,331.769258991731));
#20106=CARTESIAN_POINT('Ctrl Pts',(111.336716065975,-4.87085323337215,331.637334882168));
#20107=CARTESIAN_POINT('Ctrl Pts',(111.34411473573,-4.77955198419317,331.508774970614));
#20108=CARTESIAN_POINT('Ctrl Pts',(111.351513405484,-4.68323404309151,331.384028559276));
#20109=CARTESIAN_POINT('Ctrl Pts',(111.358910854688,-4.58693199145916,331.259302727223));
#20110=CARTESIAN_POINT('Ctrl Pts',(111.366308303892,-4.48561511828267,331.138389441927));
#20111=CARTESIAN_POINT('Ctrl Pts',(111.373705753096,-4.379625373287,331.021707382286));
#20112=CARTESIAN_POINT('Ctrl Pts',(111.38110288156,-4.27364022382189,330.905030381775));
#20113=CARTESIAN_POINT('Ctrl Pts',(111.388500010023,-4.16298285632729,330.792584518397));
#20114=CARTESIAN_POINT('Ctrl Pts',(111.395897138487,-4.04803401675782,330.684753638357));
#20115=CARTESIAN_POINT('Ctrl Pts',(111.403295405923,-3.93306747793625,330.576906155053));
#20116=CARTESIAN_POINT('Ctrl Pts',(111.41069367336,-3.81380842355036,330.473675325324));
#20117=CARTESIAN_POINT('Ctrl Pts',(111.418091940797,-3.6906726761321,330.375406422165));
#20118=CARTESIAN_POINT('Ctrl Pts',(111.425492807322,-3.56749366983102,330.277102996107));
#20119=CARTESIAN_POINT('Ctrl Pts',(111.432893673848,-3.44043555043321,330.183765199931));
#20120=CARTESIAN_POINT('Ctrl Pts',(111.440294540374,-3.30994512927636,330.095696399724));
#20121=CARTESIAN_POINT('Ctrl Pts',(111.447703533759,-3.17931141716171,330.007530891555));
#20122=CARTESIAN_POINT('Ctrl Pts',(111.455112527144,-3.04523818593642,329.924646142936));
#20123=CARTESIAN_POINT('Ctrl Pts',(111.462521520528,-2.9081996114074,329.847301136035));
#20124=CARTESIAN_POINT('Ctrl Pts',(111.469935078109,-2.77107661638961,329.769908481941));
#20125=CARTESIAN_POINT('Ctrl Pts',(111.477348635689,-2.63098496932983,329.698062539678));
#20126=CARTESIAN_POINT('Ctrl Pts',(111.484762193269,-2.4884205887163,329.631974894232));
#20127=CARTESIAN_POINT('Ctrl Pts',(111.492186305406,-2.34565324160717,329.565793160924));
#20128=CARTESIAN_POINT('Ctrl Pts',(111.499610417542,-2.2004064736915,329.505386240386));
#20129=CARTESIAN_POINT('Ctrl Pts',(111.507034529679,-2.05319395201455,329.450916728151));
#20130=CARTESIAN_POINT('Ctrl Pts',(111.510891654834,-1.97671112012507,329.422617623565));
#20131=CARTESIAN_POINT('Ctrl Pts',(111.514748779989,-1.89969791124875,329.395920327023));
#20132=CARTESIAN_POINT('Ctrl Pts',(111.518605905144,-1.82222752532369,329.370842211445));
#20133=CARTESIAN_POINT('Ctrl Pts',(111.526029882582,-1.67311688614997,329.322573265853));
#20134=CARTESIAN_POINT('Ctrl Pts',(111.53345386002,-1.52186208918751,329.280160278417));
#20135=CARTESIAN_POINT('Ctrl Pts',(111.540877837458,-1.36896395811982,329.243797411151));
#20136=CARTESIAN_POINT('Ctrl Pts',(111.548293053486,-1.21624626985155,329.20747745754));
#20137=CARTESIAN_POINT('Ctrl Pts',(111.555708269513,-1.06188946740132,329.177193497221));
#20138=CARTESIAN_POINT('Ctrl Pts',(111.563123485541,-0.906411806233638,
329.153090713888));
#20139=CARTESIAN_POINT('Ctrl Pts',(111.570531566685,-0.751083744888806,
329.129011122133));
#20140=CARTESIAN_POINT('Ctrl Pts',(111.577939647829,-0.594637338229394,
329.111100923796));
#20141=CARTESIAN_POINT('Ctrl Pts',(111.585347728973,-0.437603270357113,
329.099454776017));
#20142=CARTESIAN_POINT('Ctrl Pts',(111.592750296147,-0.28068608580945,329.087817296678));
#20143=CARTESIAN_POINT('Ctrl Pts',(111.600152863321,-0.123182481584819,
329.082434611768));
#20144=CARTESIAN_POINT('Ctrl Pts',(111.607555430495,0.034369565853609,329.083349824821));
#20145=CARTESIAN_POINT('Ctrl Pts',(111.61495410025,0.191838662827861,329.084264556018));
#20146=CARTESIAN_POINT('Ctrl Pts',(111.622352770005,0.349355779955852,329.091470579372));
#20147=CARTESIAN_POINT('Ctrl Pts',(111.629751439759,0.506380863250504,329.104958949775));
#20148=CARTESIAN_POINT('Ctrl Pts',(111.637148888963,0.66338004228219,329.118445095017));
#20149=CARTESIAN_POINT('Ctrl Pts',(111.644546338167,0.819886977096974,329.138211498495));
#20150=CARTESIAN_POINT('Ctrl Pts',(111.651943787371,0.975364543059989,329.164197178567));
#20151=CARTESIAN_POINT('Ctrl Pts',(111.659340915835,1.13083536778669,329.190181731946));
#20152=CARTESIAN_POINT('Ctrl Pts',(111.666738044298,1.28527654429864,329.222384964228));
#20153=CARTESIAN_POINT('Ctrl Pts',(111.674135172762,1.43815924464937,329.260694419224));
#20154=CARTESIAN_POINT('Ctrl Pts',(111.681533440198,1.5910654851196,329.29900977292));
#20155=CARTESIAN_POINT('Ctrl Pts',(111.688931707635,1.74241240958322,329.343433130683));
#20156=CARTESIAN_POINT('Ctrl Pts',(111.696329975071,1.89168464518075,329.393801665506));
#20157=CARTESIAN_POINT('Ctrl Pts',(111.703730841597,2.04100932168454,329.444187895324));
#20158=CARTESIAN_POINT('Ctrl Pts',(111.711131708123,2.18825750476337,329.50052334136));
#20159=CARTESIAN_POINT('Ctrl Pts',(111.718532574649,2.33293229214959,329.562596439223));
#20160=CARTESIAN_POINT('Ctrl Pts',(111.725941568033,2.47776594628382,329.624737699283));
#20161=CARTESIAN_POINT('Ctrl Pts',(111.733350561418,2.62002021820294,329.692629046344));
#20162=CARTESIAN_POINT('Ctrl Pts',(111.740759554803,2.7592207205391,329.766011885966));
#20163=CARTESIAN_POINT('Ctrl Pts',(111.748173112383,2.89850697518625,329.839439931949));
#20164=CARTESIAN_POINT('Ctrl Pts',(111.755586669963,3.03473538948241,329.918366024808));
#20165=CARTESIAN_POINT('Ctrl Pts',(111.763000227544,3.16745966714886,330.002487636885));
#20166=CARTESIAN_POINT('Ctrl Pts',(111.77042433968,3.3003729021229,330.086729011477));
#20167=CARTESIAN_POINT('Ctrl Pts',(111.777848451817,3.42977173070535,330.176180466471));
#20168=CARTESIAN_POINT('Ctrl Pts',(111.785272563954,3.55524144813195,330.270498038061));
#20169=CARTESIAN_POINT('Ctrl Pts',(111.789129689108,3.62042801782811,330.319499813789));
#20170=CARTESIAN_POINT('Ctrl Pts',(111.792986814263,3.68455461038738,330.369814425085));
#20171=CARTESIAN_POINT('Ctrl Pts',(111.796843939418,3.74756700386472,330.421389718043));
#20172=CARTESIAN_POINT('Ctrl Pts',(111.804267916856,3.86884971280862,330.520658939529));
#20173=CARTESIAN_POINT('Ctrl Pts',(111.811691894294,3.98636834841945,330.624900224016));
#20174=CARTESIAN_POINT('Ctrl Pts',(111.819115871732,4.09968861128476,330.73379749039));
#20175=CARTESIAN_POINT('Ctrl Pts',(111.826531087759,4.21287513918994,330.842566241606));
#20176=CARTESIAN_POINT('Ctrl Pts',(111.833946303787,4.32187289029909,330.955979781222));
#20177=CARTESIAN_POINT('Ctrl Pts',(111.841361519814,4.42627931877771,331.07368086439));
#20178=CARTESIAN_POINT('Ctrl Pts',(111.848769600958,4.53058528791646,331.191268696167));
#20179=CARTESIAN_POINT('Ctrl Pts',(111.856177682103,4.63030848333096,331.313135581158));
#20180=CARTESIAN_POINT('Ctrl Pts',(111.863585763247,4.72508212219692,331.438886480187));
#20181=CARTESIAN_POINT('Ctrl Pts',(111.870988330421,4.81978521931264,331.564543780525));
#20182=CARTESIAN_POINT('Ctrl Pts',(111.878390897595,4.90954587168814,331.694079041847));
#20183=CARTESIAN_POINT('Ctrl Pts',(111.885793464769,4.99403670271017,331.827063194061));
#20184=CARTESIAN_POINT('Ctrl Pts',(111.893192134523,5.07848304967887,331.9599773307));
#20185=CARTESIAN_POINT('Ctrl Pts',(111.900590804278,5.15766490131545,332.09633642769));
#20186=CARTESIAN_POINT('Ctrl Pts',(111.907989474033,5.23129752554913,332.235681501403));
#20187=CARTESIAN_POINT('Ctrl Pts',(111.915386923237,5.30491800268633,332.375003587506));
#20188=CARTESIAN_POINT('Ctrl Pts',(111.922784372441,5.37299089509791,332.517310343039));
#20189=CARTESIAN_POINT('Ctrl Pts',(111.930181821645,5.43527681458859,332.66211708777));
#20190=CARTESIAN_POINT('Ctrl Pts',(111.937578950108,5.49756003347035,332.806917553934));
#20191=CARTESIAN_POINT('Ctrl Pts',(111.944976078572,5.55405663086222,332.954217450929));
#20192=CARTESIAN_POINT('Ctrl Pts',(111.952373207035,5.60457499442688,333.103511219557));
#20193=CARTESIAN_POINT('Ctrl Pts',(111.959771474472,5.65510113655845,333.252827975699));
#20194=CARTESIAN_POINT('Ctrl Pts',(111.967169741908,5.69964709239634,333.404138861223));
#20195=CARTESIAN_POINT('Ctrl Pts',(111.974568009345,5.73807088881975,333.556922373058));
#20196=CARTESIAN_POINT('Ctrl Pts',(111.981968875871,5.77650818392695,333.709759559348));
#20197=CARTESIAN_POINT('Ctrl Pts',(111.989369742396,5.80881894645461,333.864070040278));
#20198=CARTESIAN_POINT('Ctrl Pts',(111.996770608922,5.83491218308189,334.0193214705));
#20199=CARTESIAN_POINT('Ctrl Pts',(112.004179602307,5.86103407257759,334.174743381634));
#20200=CARTESIAN_POINT('Ctrl Pts',(112.011588595692,5.88092473951966,334.331107937252));
#20201=CARTESIAN_POINT('Ctrl Pts',(112.018997589076,5.89454492326482,334.487876274605));
#20202=CARTESIAN_POINT('Ctrl Pts',(112.026411146657,5.90817349751299,334.64474118666));
#20203=CARTESIAN_POINT('Ctrl Pts',(112.033824704237,5.91552387397367,334.802010004172));
#20204=CARTESIAN_POINT('Ctrl Pts',(112.041238261817,5.91660893808531,334.959143712002));
#20205=CARTESIAN_POINT('Ctrl Pts',(112.048662373954,5.91769554698436,335.116501128431));
#20206=CARTESIAN_POINT('Ctrl Pts',(112.056086486091,5.91249904116674,335.273722679009));
#20207=CARTESIAN_POINT('Ctrl Pts',(112.063510598227,5.90108424659031,335.4302734911));
#20208=CARTESIAN_POINT('Ctrl Pts',(112.067367723382,5.89515380124041,335.511607940825));
#20209=CARTESIAN_POINT('Ctrl Pts',(112.071224848537,5.88754575000308,335.592761483817));
#20210=CARTESIAN_POINT('Ctrl Pts',(112.075081973692,5.87827460760497,335.673660300216));
#20211=CARTESIAN_POINT('Ctrl Pts',(112.08250595113,5.86043003445131,335.829369789433));
#20212=CARTESIAN_POINT('Ctrl Pts',(112.089929928568,5.83636739138287,335.984604657669));
#20213=CARTESIAN_POINT('Ctrl Pts',(112.097353906006,5.80611745341878,336.138828643654));
#20214=CARTESIAN_POINT('Ctrl Pts',(112.104769122033,5.77590321493284,336.292870622131));
#20215=CARTESIAN_POINT('Ctrl Pts',(112.112184338061,5.7395162873123,336.445903730358));
#20216=CARTESIAN_POINT('Ctrl Pts',(112.119599554089,5.69703924472344,336.597396133268));
#20217=CARTESIAN_POINT('Ctrl Pts',(112.127007635233,5.65460307333107,336.748742770951));
#20218=CARTESIAN_POINT('Ctrl Pts',(112.134415716377,5.60608855298068,336.898551297666));
#20219=CARTESIAN_POINT('Ctrl Pts',(112.141823797521,5.55162939330956,337.046299499546));
#20220=CARTESIAN_POINT('Ctrl Pts',(112.149226364695,5.4972107685856,337.19393772974));
#20221=CARTESIAN_POINT('Ctrl Pts',(112.156628931869,5.43685644329193,337.339518339916));
#20222=CARTESIAN_POINT('Ctrl Pts',(112.164031499043,5.37075006935111,337.482533837648));
#20223=CARTESIAN_POINT('Ctrl Pts',(112.171430168798,5.30467850012722,337.625474038345));
#20224=CARTESIAN_POINT('Ctrl Pts',(112.178828838553,5.23286106974775,337.765851478322));
#20225=CARTESIAN_POINT('Ctrl Pts',(112.186227508307,5.15552966247693,337.903178337929));
#20226=CARTESIAN_POINT('Ctrl Pts',(112.193624957511,5.07821101248703,338.040482542868));
#20227=CARTESIAN_POINT('Ctrl Pts',(112.201022406715,4.99538037388325,338.174736841347));
#20228=CARTESIAN_POINT('Ctrl Pts',(112.208419855919,4.90731577792332,338.305477638443));
#20229=CARTESIAN_POINT('Ctrl Pts',(112.215816984383,4.81925500029074,338.436212766845));
#20230=CARTESIAN_POINT('Ctrl Pts',(112.223214112846,4.72596092502395,338.563434387225));
#20231=CARTESIAN_POINT('Ctrl Pts',(112.23061124131,4.62775499520856,338.686707781588));
#20232=CARTESIAN_POINT('Ctrl Pts',(112.238009508747,4.52953394413146,338.810000156977));
#20233=CARTESIAN_POINT('Ctrl Pts',(112.245407776183,4.42639976516784,338.929342803961));
#20234=CARTESIAN_POINT('Ctrl Pts',(112.25280604362,4.31871417157305,339.04433411908));
#20235=CARTESIAN_POINT('Ctrl Pts',(112.260206910146,4.21099074689679,339.159365831857));
#20236=CARTESIAN_POINT('Ctrl Pts',(112.267607776671,4.09871297900713,339.270042896951));
#20237=CARTESIAN_POINT('Ctrl Pts',(112.275008643197,3.98227928675753,339.376000713524));
#20238=CARTESIAN_POINT('Ctrl Pts',(112.282417636582,3.86571773918234,339.482074881909));
#20239=CARTESIAN_POINT('Ctrl Pts',(112.289826629967,3.74499142967971,339.583419201331));
#20240=CARTESIAN_POINT('Ctrl Pts',(112.297235623351,3.6205322532438,339.679709047123));
#20241=CARTESIAN_POINT('Ctrl Pts',(112.304649180932,3.49599640566206,339.776058210781));
#20242=CARTESIAN_POINT('Ctrl Pts',(112.312062738512,3.36772341229982,339.867346480399));
#20243=CARTESIAN_POINT('Ctrl Pts',(112.319476296092,3.23617351553603,339.953292999596));
#20244=CARTESIAN_POINT('Ctrl Pts',(112.326900408229,3.10443633341096,340.039361879397));
#20245=CARTESIAN_POINT('Ctrl Pts',(112.334324520366,2.96941324988094,340.120073629181));
#20246=CARTESIAN_POINT('Ctrl Pts',(112.341748632502,2.83158913180129,340.195193312204));
#20247=CARTESIAN_POINT('Ctrl Pts',(112.345605757657,2.75998395357303,340.2342210119));
#20248=CARTESIAN_POINT('Ctrl Pts',(112.349462882811,2.68762305486854,340.271740078002));
#20249=CARTESIAN_POINT('Ctrl Pts',(112.353320007966,2.61457636713573,340.307722768091));
#20250=CARTESIAN_POINT('Ctrl Pts',(112.360743985404,2.47398021328188,340.376980225053));
#20251=CARTESIAN_POINT('Ctrl Pts',(112.368167962842,2.33041822391381,340.44075192972));
#20252=CARTESIAN_POINT('Ctrl Pts',(112.37559194028,2.18435800670142,340.498773559719));
#20253=CARTESIAN_POINT('Ctrl Pts',(112.383007156307,2.0384701625215,340.556726715464));
#20254=CARTESIAN_POINT('Ctrl Pts',(112.390422372335,1.89009030257854,340.608943167646));
#20255=CARTESIAN_POINT('Ctrl Pts',(112.397837588363,1.739710343946,340.655204548172));
#20256=CARTESIAN_POINT('Ctrl Pts',(112.405245669507,1.58947508015237,340.701421416231));
#20257=CARTESIAN_POINT('Ctrl Pts',(112.412653750651,1.4372439032895,340.741694510873));
#20258=CARTESIAN_POINT('Ctrl Pts',(112.420061831795,1.28352831209565,340.775853671497));
#20259=CARTESIAN_POINT('Ctrl Pts',(112.427464398969,1.12992713422372,340.809987406835));
#20260=CARTESIAN_POINT('Ctrl Pts',(112.434866966143,0.974844104754665,340.838016188672));
#20261=CARTESIAN_POINT('Ctrl Pts',(112.442269533317,0.818805369488226,340.859819820557));
#20262=CARTESIAN_POINT('Ctrl Pts',(112.449668203072,0.662848787933832,340.881611972926));
#20263=CARTESIAN_POINT('Ctrl Pts',(112.457066872826,0.505937871374166,340.89718545119));
#20264=CARTESIAN_POINT('Ctrl Pts',(112.464465542581,0.348608323641791,340.90647126457));
#20265=CARTESIAN_POINT('Ctrl Pts',(112.471862991785,0.191304730399448,340.915755546078));
#20266=CARTESIAN_POINT('Ctrl Pts',(112.479260440989,0.0335830152491352,
340.91875419938));
#20267=CARTESIAN_POINT('Ctrl Pts',(112.486657890193,-0.12401651627988,340.915450149075));
#20268=CARTESIAN_POINT('Ctrl Pts',(112.494055018657,-0.281609214567851,
340.912146242028));
#20269=CARTESIAN_POINT('Ctrl Pts',(112.50145214712,-0.43907936663873,340.902540182557));
#20270=CARTESIAN_POINT('Ctrl Pts',(112.508849275583,-0.595887457559155,
340.88666702816));
#20271=CARTESIAN_POINT('Ctrl Pts',(112.51624754302,-0.752719693011461,340.870791429693));
#20272=CARTESIAN_POINT('Ctrl Pts',(112.523645810457,-0.90888929299925,340.848646852494));
#20273=CARTESIAN_POINT('Ctrl Pts',(112.531044077893,-1.0638627968066,340.82032013828));
#20274=CARTESIAN_POINT('Ctrl Pts',(112.538444944419,-1.21889074443568,340.791983472594));
#20275=CARTESIAN_POINT('Ctrl Pts',(112.545845810945,-1.37272139236702,340.757460412805));
#20276=CARTESIAN_POINT('Ctrl Pts',(112.553246677471,-1.52483253267406,340.716888691395));
#20277=CARTESIAN_POINT('Ctrl Pts',(112.560655670855,-1.67711070555533,340.676272418355));
#20278=CARTESIAN_POINT('Ctrl Pts',(112.56806466424,-1.82766523918877,340.629594315487));
#20279=CARTESIAN_POINT('Ctrl Pts',(112.575473657625,-1.97598942660418,340.57704189947));
#20280=CARTESIAN_POINT('Ctrl Pts',(112.582887215205,-2.12440498683539,340.524457109353));
#20281=CARTESIAN_POINT('Ctrl Pts',(112.590300772785,-2.27058711731749,340.46599093346));
#20282=CARTESIAN_POINT('Ctrl Pts',(112.597714330366,-2.41405057636902,340.401878411926));
#20283=CARTESIAN_POINT('Ctrl Pts',(112.605138442502,-2.5577182819189,340.33767461448));
#20284=CARTESIAN_POINT('Ctrl Pts',(112.612562554639,-2.69865925234245,340.267808581996));
#20285=CARTESIAN_POINT('Ctrl Pts',(112.619986666776,-2.83641353504342,340.192560911604));
#20286=CARTESIAN_POINT('Ctrl Pts',(112.62384379193,-2.90798243098363,340.153466717316));
#20287=CARTESIAN_POINT('Ctrl Pts',(112.627700917085,-2.97869164846253,340.112920613353));
#20288=CARTESIAN_POINT('Ctrl Pts',(112.631558042239,-3.04848001436847,340.070966393548));
#20289=CARTESIAN_POINT('Ctrl Pts',(112.638982019677,-3.18280473372633,339.99021527224));
#20290=CARTESIAN_POINT('Ctrl Pts',(112.646405997115,-3.31412135072215,339.904001461234));
#20291=CARTESIAN_POINT('Ctrl Pts',(112.653829974553,-3.44195454169205,339.812575141795));
#20292=CARTESIAN_POINT('Ctrl Pts',(112.661245190581,-3.56963687026307,339.721256719169));
#20293=CARTESIAN_POINT('Ctrl Pts',(112.668660406609,-3.69384365514196,339.624738247853));
#20294=CARTESIAN_POINT('Ctrl Pts',(112.676075622636,-3.81412506138573,339.523315219903));
#20295=CARTESIAN_POINT('Ctrl Pts',(112.68348370378,-3.93429073346604,339.421989780681));
#20296=CARTESIAN_POINT('Ctrl Pts',(112.690891784924,-4.05053826276284,339.315769418728));
#20297=CARTESIAN_POINT('Ctrl Pts',(112.698299866068,-4.16244775627929,339.204992180581));
#20298=CARTESIAN_POINT('Ctrl Pts',(112.705702433242,-4.27427395351608,339.094297395955));
#20299=CARTESIAN_POINT('Ctrl Pts',(112.713105000416,-4.38176828003886,338.979052750067));
#20300=CARTESIAN_POINT('Ctrl Pts',(112.72050756759,-4.48454493240522,338.859635644946));
#20301=CARTESIAN_POINT('Ctrl Pts',(112.727906237345,-4.58726747331329,338.74028141241));
#20302=CARTESIAN_POINT('Ctrl Pts',(112.7353049071,-4.68527704392799,338.616759377822));
#20303=CARTESIAN_POINT('Ctrl Pts',(112.742703576854,-4.77822572834857,338.489482691094));
#20304=CARTESIAN_POINT('Ctrl Pts',(112.750101026058,-4.8711590791223,338.362227001069));
#20305=CARTESIAN_POINT('Ctrl Pts',(112.757498475262,-4.95903298079465,338.231218189318));
#20306=CARTESIAN_POINT('Ctrl Pts',(112.764895924466,-5.04154068397413,338.09690136981));
#20307=CARTESIAN_POINT('Ctrl Pts',(112.77229305293,-5.12404480976344,337.962590374046));
#20308=CARTESIAN_POINT('Ctrl Pts',(112.779690181393,-5.20118300433905,337.824971973716));
#20309=CARTESIAN_POINT('Ctrl Pts',(112.787087309857,-5.27269278581095,337.684518830062));
#20310=CARTESIAN_POINT('Ctrl Pts',(112.794485577293,-5.34421357800407,337.54404406013));
#20311=CARTESIAN_POINT('Ctrl Pts',(112.80188384473,-5.410104062167,337.40073401039));
#20312=CARTESIAN_POINT('Ctrl Pts',(112.809282112166,-5.47014857914836,337.255084274377));
#20313=CARTESIAN_POINT('Ctrl Pts',(112.816682978692,-5.53021419040002,337.109383370079));
#20314=CARTESIAN_POINT('Ctrl Pts',(112.824083845218,-5.58442960330336,336.961341487817));
#20315=CARTESIAN_POINT('Ctrl Pts',(112.831484711744,-5.63262804336511,336.811472298324));
#20316=CARTESIAN_POINT('Ctrl Pts',(112.838893705128,-5.680879409922,336.661438538134));
#20317=CARTESIAN_POINT('Ctrl Pts',(112.846302698513,-5.72310049435268,336.50957381901));
#20318=CARTESIAN_POINT('Ctrl Pts',(112.853711691898,-5.7591747752185,336.356405717692));
#20319=CARTESIAN_POINT('Ctrl Pts',(112.861125249478,-5.79527127908566,336.203143259539));
#20320=CARTESIAN_POINT('Ctrl Pts',(112.868538807058,-5.82521336318953,336.048576184795));
#20321=CARTESIAN_POINT('Ctrl Pts',(112.875952364639,-5.84893608567506,335.893239737242));
#20322=CARTESIAN_POINT('Ctrl Pts',(112.883376476775,-5.87269258179906,335.737682139818));
#20323=CARTESIAN_POINT('Ctrl Pts',(112.890800588912,-5.89021199084438,335.581353351856));
#20324=CARTESIAN_POINT('Ctrl Pts',(112.898224701049,-5.90148136618252,335.424792004516));
#20325=CARTESIAN_POINT('Ctrl Pts',(112.902081826204,-5.90733626038337,335.343452081306));
#20326=CARTESIAN_POINT('Ctrl Pts',(112.905938951358,-5.91150499142025,335.26204936842));
#20327=CARTESIAN_POINT('Ctrl Pts',(112.909796076513,-5.91399128217944,335.180659006987));
#20328=CARTESIAN_POINT('Ctrl Pts',(112.912631257774,-5.91581883111431,335.12083299195));
#20329=CARTESIAN_POINT('Ctrl Pts',(112.915466439034,-5.9167386071917,335.060979105019));
#20330=CARTESIAN_POINT('Ctrl Pts',(112.918301620294,-5.91674989481959,335.001115639915));
#20331=CARTESIAN_POINT('',(114.668301620294,-5.91183534194015,335.004818938716));
#20332=CARTESIAN_POINT('Ctrl Pts',(112.918302791716,-5.92624301184832,335.001092656212));
#20333=CARTESIAN_POINT('Ctrl Pts',(113.008213231406,-5.92131010852706,333.099630750775));
#20334=CARTESIAN_POINT('Ctrl Pts',(113.190869682522,-3.8962064387588,329.227734848842));
#20335=CARTESIAN_POINT('Ctrl Pts',(113.46627214506,2.70289327938773,328.546552019156));
#20336=CARTESIAN_POINT('Ctrl Pts',(113.744510179335,6.88953273082826,333.780589621136));
#20337=CARTESIAN_POINT('Ctrl Pts',(114.022748213608,4.7537496845221,340.133662129328));
#20338=CARTESIAN_POINT('Ctrl Pts',(114.300986247883,-1.74447928203647,341.775648674169));
#20339=CARTESIAN_POINT('Ctrl Pts',(114.516170716778,-5.5320017806064,338.236706706155));
#20340=CARTESIAN_POINT('Ctrl Pts',(114.638609174248,-5.91666024635598,335.636725282272));
#20341=CARTESIAN_POINT('Ctrl Pts',(114.668301620294,-5.91183534194015,335.004818938716));
#20342=CARTESIAN_POINT('',(116.418301620294,-5.90886619475503,334.996662217394));
#20343=CARTESIAN_POINT('Ctrl Pts',(114.668301620294,-5.91183534194015,335.004818938716));
#20344=CARTESIAN_POINT('Ctrl Pts',(114.731355185673,-5.90158938828715,333.662930571381));
#20345=CARTESIAN_POINT('Ctrl Pts',(114.887154762477,-4.78309971499823,330.33179209936));
#20346=CARTESIAN_POINT('Ctrl Pts',(115.135700350704,0.74963200781035,328.043659383405));
#20347=CARTESIAN_POINT('Ctrl Pts',(115.413938384979,6.25540412481643,331.865906485686));
#20348=CARTESIAN_POINT('Ctrl Pts',(115.692176419252,6.0206842060895,338.564264946907));
#20349=CARTESIAN_POINT('Ctrl Pts',(115.970414453527,0.260871256591412,341.991750074816));
#20350=CARTESIAN_POINT('Ctrl Pts',(116.212456187207,-4.95789529531347,339.391818017654));
#20351=CARTESIAN_POINT('Ctrl Pts',(116.361751909463,-5.90270235742463,336.201657451435));
#20352=CARTESIAN_POINT('Ctrl Pts',(116.418301620294,-5.90886619475503,334.996662217394));
#20353=CARTESIAN_POINT('',(118.168300196814,-5.92087836980671,334.996633443784));
#20354=CARTESIAN_POINT('Ctrl Pts',(116.418301620294,-5.90886619475503,334.996662217394));
#20355=CARTESIAN_POINT('Ctrl Pts',(116.454497920888,-5.91281153957713,334.225369684439));
#20356=CARTESIAN_POINT('Ctrl Pts',(116.583440232905,-5.41355607546623,331.482697059055));
#20357=CARTESIAN_POINT('Ctrl Pts',(116.805128556348,-1.2659262506568,328.118862474187));
#20358=CARTESIAN_POINT('Ctrl Pts',(117.083366590623,5.10143001502218,330.211677253667));
#20359=CARTESIAN_POINT('Ctrl Pts',(117.361604624895,6.7872792528987,336.698665141928));
#20360=CARTESIAN_POINT('Ctrl Pts',(117.63984265917,2.24454250046778,341.626813101694));
#20361=CARTESIAN_POINT('Ctrl Pts',(117.908740818052,-4.13634482415734,340.512342377915));
#20362=CARTESIAN_POINT('Ctrl Pts',(118.084892965511,-5.91195779426516,336.762288914003));
#20363=CARTESIAN_POINT('Ctrl Pts',(118.168299101544,-5.92405561514005,334.99665480686));
#20364=CARTESIAN_POINT('',(119.918302439026,-5.91853562323323,335.00514099704));
#20365=CARTESIAN_POINT('Ctrl Pts',(118.168301620294,-5.91674902637294,334.996605679018));
#20366=CARTESIAN_POINT('Ctrl Pts',(118.177640656102,-5.9166357507117,334.799151265657));
#20367=CARTESIAN_POINT('Ctrl Pts',(118.18697969191,-5.90663908245873,334.601984314875));
#20368=CARTESIAN_POINT('Ctrl Pts',(118.196318727718,-5.88683994509542,334.405823238986));
#20369=CARTESIAN_POINT('Ctrl Pts',(118.203742705156,-5.87110080969631,334.249886862729));
#20370=CARTESIAN_POINT('Ctrl Pts',(118.211166682594,-5.84913775930447,334.094341051069));
#20371=CARTESIAN_POINT('Ctrl Pts',(118.218590660032,-5.82097432064191,333.93972243213));
#20372=CARTESIAN_POINT('Ctrl Pts',(118.22600587606,-5.79284411907441,333.785286286426));
#20373=CARTESIAN_POINT('Ctrl Pts',(118.233421092088,-5.7585281608484,333.631775518965));
#20374=CARTESIAN_POINT('Ctrl Pts',(118.240836308115,-5.71810182690776,333.47972303194));
#20375=CARTESIAN_POINT('Ctrl Pts',(118.248244389259,-5.67771439098206,333.327816849052));
#20376=CARTESIAN_POINT('Ctrl Pts',(118.255652470403,-5.63122837933056,333.177366511459));
#20377=CARTESIAN_POINT('Ctrl Pts',(118.263060551548,-5.57877043369371,333.028895991926));
#20378=CARTESIAN_POINT('Ctrl Pts',(118.270463118722,-5.52635153346386,332.880535981713));
#20379=CARTESIAN_POINT('Ctrl Pts',(118.277865685896,-5.46796967372883,332.734153205764));
#20380=CARTESIAN_POINT('Ctrl Pts',(118.28526825307,-5.40380163285874,332.590257591523));
#20381=CARTESIAN_POINT('Ctrl Pts',(118.292666922824,-5.33966737618174,332.446437737694));
#20382=CARTESIAN_POINT('Ctrl Pts',(118.300065592579,-5.2697531570709,332.305102777663));
#20383=CARTESIAN_POINT('Ctrl Pts',(118.307464262334,-5.19428424763646,332.166743619569));
#20384=CARTESIAN_POINT('Ctrl Pts',(118.314861711538,-5.11882778822859,332.028407286439));
#20385=CARTESIAN_POINT('Ctrl Pts',(118.322259160742,-5.03781863569839,331.89304610826));
#20386=CARTESIAN_POINT('Ctrl Pts',(118.329656609946,-4.95152853224047,331.761127394153));
#20387=CARTESIAN_POINT('Ctrl Pts',(118.337053738409,-4.86524217017103,331.629214399811));
#20388=CARTESIAN_POINT('Ctrl Pts',(118.344450866873,-4.77367551674591,331.500743885091));
#20389=CARTESIAN_POINT('Ctrl Pts',(118.351847995336,-4.67714411218454,331.376154871361));
#20390=CARTESIAN_POINT('Ctrl Pts',(118.359246262773,-4.5805978441965,331.251546674034));
#20391=CARTESIAN_POINT('Ctrl Pts',(118.366644530209,-4.47908553155157,331.130821462744));
#20392=CARTESIAN_POINT('Ctrl Pts',(118.374042797646,-4.37296342837738,331.014385691443));
#20393=CARTESIAN_POINT('Ctrl Pts',(118.381443664171,-4.26680404339248,330.897909015032));
#20394=CARTESIAN_POINT('Ctrl Pts',(118.388844530697,-4.15603189476303,330.785725054556));
#20395=CARTESIAN_POINT('Ctrl Pts',(118.396245397223,-4.04104043881098,330.678203760658));
#20396=CARTESIAN_POINT('Ctrl Pts',(118.403654390607,-3.92592271124648,330.570564398099));
#20397=CARTESIAN_POINT('Ctrl Pts',(118.411063383992,-3.80657669637475,330.467598182187));
#20398=CARTESIAN_POINT('Ctrl Pts',(118.418472377377,-3.68342986372551,330.369635543338));
#20399=CARTESIAN_POINT('Ctrl Pts',(118.425885934957,-3.5602071683796,330.271612556126));
#20400=CARTESIAN_POINT('Ctrl Pts',(118.433299492537,-3.43317929005262,330.17859950799));
#20401=CARTESIAN_POINT('Ctrl Pts',(118.440713050118,-3.30280263442986,330.090883448063));
#20402=CARTESIAN_POINT('Ctrl Pts',(118.448137162254,-3.17224036376924,330.003042508266));
#20403=CARTESIAN_POINT('Ctrl Pts',(118.455561274391,-3.03832011083527,329.920513813298));
#20404=CARTESIAN_POINT('Ctrl Pts',(118.462985386528,-2.90152352396745,329.84353882955));
#20405=CARTESIAN_POINT('Ctrl Pts',(118.466842511682,-2.83045218956942,329.803547226429));
#20406=CARTESIAN_POINT('Ctrl Pts',(118.470699636837,-2.75860482035376,329.765053908568));
#20407=CARTESIAN_POINT('Ctrl Pts',(118.474556761991,-2.68605096655409,329.728087560707));
#20408=CARTESIAN_POINT('Ctrl Pts',(118.481980739429,-2.54640339172725,329.656936814624));
#20409=CARTESIAN_POINT('Ctrl Pts',(118.489404716867,-2.40371613347195,329.591231248354));
#20410=CARTESIAN_POINT('Ctrl Pts',(118.496828694305,-2.25845318548505,329.531241478043));
#20411=CARTESIAN_POINT('Ctrl Pts',(118.504243910333,-2.11336166963261,329.471322504688));
#20412=CARTESIAN_POINT('Ctrl Pts',(118.511659126361,-1.96570085622135,329.417106041341));
#20413=CARTESIAN_POINT('Ctrl Pts',(118.519074342388,-1.8159596670263,329.36881708251));
#20414=CARTESIAN_POINT('Ctrl Pts',(118.526482423532,-1.6663625580496,329.320574587072));
#20415=CARTESIAN_POINT('Ctrl Pts',(118.533890504676,-1.51468941117923,329.278248355495));
#20416=CARTESIAN_POINT('Ctrl Pts',(118.54129858582,-1.36144937940466,329.242015443767));
#20417=CARTESIAN_POINT('Ctrl Pts',(118.548701152994,-1.20832340698424,329.205809500856));
#20418=CARTESIAN_POINT('Ctrl Pts',(118.556103720168,-1.05363323349634,329.175687932722));
#20419=CARTESIAN_POINT('Ctrl Pts',(118.563506287342,-0.897903332726364,
329.15177803366));
#20420=CARTESIAN_POINT('Ctrl Pts',(118.570904957097,-0.742255423068583,
329.127880723056));
#20421=CARTESIAN_POINT('Ctrl Pts',(118.578303626852,-0.585569244291613,
329.110188624789));
#20422=CARTESIAN_POINT('Ctrl Pts',(118.585702296607,-0.428379519186952,
329.0987779613));
#20423=CARTESIAN_POINT('Ctrl Pts',(118.593099745811,-0.271215725506044,
329.087369180215));
#20424=CARTESIAN_POINT('Ctrl Pts',(118.600497195015,-0.113548922233473,
329.082239804297));
#20425=CARTESIAN_POINT('Ctrl Pts',(118.607894644219,0.0440808651278728,
329.083414207515));
#20426=CARTESIAN_POINT('Ctrl Pts',(118.615291772682,0.201703817936448,329.084588559814));
#20427=CARTESIAN_POINT('Ctrl Pts',(118.622688901146,0.359289384824021,329.092066145016));
#20428=CARTESIAN_POINT('Ctrl Pts',(118.630086029609,0.516297626437871,329.105819198274));
#20429=CARTESIAN_POINT('Ctrl Pts',(118.637484297046,0.673330043401532,329.119574369159));
#20430=CARTESIAN_POINT('Ctrl Pts',(118.644882564482,0.829784586282144,329.139606899491));
#20431=CARTESIAN_POINT('Ctrl Pts',(118.652280831919,0.985126669729223,329.165837163132));
#20432=CARTESIAN_POINT('Ctrl Pts',(118.659681698445,1.14052332648389,329.192076641741));
#20433=CARTESIAN_POINT('Ctrl Pts',(118.667082564971,1.29480637791557,329.224518126616));
#20434=CARTESIAN_POINT('Ctrl Pts',(118.674483431496,1.44745180284501,329.263030953462));
#20435=CARTESIAN_POINT('Ctrl Pts',(118.681892424881,1.60026484704455,329.301586071073));
#20436=CARTESIAN_POINT('Ctrl Pts',(118.689301418266,1.75143631141262,329.346225753484));
#20437=CARTESIAN_POINT('Ctrl Pts',(118.696710411651,1.90045700167132,329.396769347305));
#20438=CARTESIAN_POINT('Ctrl Pts',(118.704123969231,2.0495694938156,329.447344077724));
#20439=CARTESIAN_POINT('Ctrl Pts',(118.711537526811,2.19652822415995,329.503829833196));
#20440=CARTESIAN_POINT('Ctrl Pts',(118.718951084391,2.34084481966104,329.5659981512));
#20441=CARTESIAN_POINT('Ctrl Pts',(118.726375196528,2.4853668762563,329.628254977186));
#20442=CARTESIAN_POINT('Ctrl Pts',(118.733799308665,2.62723894973204,329.696210362598));
#20443=CARTESIAN_POINT('Ctrl Pts',(118.741223420802,2.76599733829589,329.769589950392));
#20444=CARTESIAN_POINT('Ctrl Pts',(118.745080545956,2.83808790766069,329.807713600562));
#20445=CARTESIAN_POINT('Ctrl Pts',(118.748937671111,2.90933849395444,329.847300643093));
#20446=CARTESIAN_POINT('Ctrl Pts',(118.752794796266,2.97968733794584,329.888308114666));
#20447=CARTESIAN_POINT('Ctrl Pts',(118.760218773704,3.11509083397726,329.967236988254));
#20448=CARTESIAN_POINT('Ctrl Pts',(118.767642751142,3.24756030925623,330.051668695727));
#20449=CARTESIAN_POINT('Ctrl Pts',(118.77506672858,3.37661710327811,330.141359500812));
#20450=CARTESIAN_POINT('Ctrl Pts',(118.782481944608,3.50552159086535,330.230944457252));
#20451=CARTESIAN_POINT('Ctrl Pts',(118.789897160635,3.63102111046476,330.325775946197));
#20452=CARTESIAN_POINT('Ctrl Pts',(118.797312376663,3.7526618757666,330.425564580337));
#20453=CARTESIAN_POINT('Ctrl Pts',(118.804720457807,3.87418559893657,330.525257198355));
#20454=CARTESIAN_POINT('Ctrl Pts',(118.812128538951,3.99185767283532,330.629897230779));
#20455=CARTESIAN_POINT('Ctrl Pts',(118.819536620095,4.10525367540771,330.739152335151));
#20456=CARTESIAN_POINT('Ctrl Pts',(118.826939187269,4.21856527526431,330.848326118953));
#20457=CARTESIAN_POINT('Ctrl Pts',(118.834341754443,4.32760687351862,330.962107877117));
#20458=CARTESIAN_POINT('Ctrl Pts',(118.841744321617,4.4319876028216,331.080125454694));
#20459=CARTESIAN_POINT('Ctrl Pts',(118.849142991372,4.53631337612679,331.198080896533));
#20460=CARTESIAN_POINT('Ctrl Pts',(118.856541661127,4.63598292099064,331.320267437476));
#20461=CARTESIAN_POINT('Ctrl Pts',(118.863940330882,4.73064277115367,331.446276666054));
#20462=CARTESIAN_POINT('Ctrl Pts',(118.871337780085,4.82528700538084,331.572265107023));
#20463=CARTESIAN_POINT('Ctrl Pts',(118.878735229289,4.91492296119113,331.702074685936));
#20464=CARTESIAN_POINT('Ctrl Pts',(118.886132678493,4.99923790320661,331.835264473982));
#20465=CARTESIAN_POINT('Ctrl Pts',(118.893529806957,5.08354918947314,331.96844848715));
#20466=CARTESIAN_POINT('Ctrl Pts',(118.90092693542,5.16253972104985,332.105012102704));
#20467=CARTESIAN_POINT('Ctrl Pts',(118.908324063884,5.23594065382523,332.244486248969));
#20468=CARTESIAN_POINT('Ctrl Pts',(118.915722331321,5.30935288851201,332.383981870771));
#20469=CARTESIAN_POINT('Ctrl Pts',(118.923120598757,5.37717363689238,332.526388585321));
#20470=CARTESIAN_POINT('Ctrl Pts',(118.930518866194,5.43918056347867,332.671213758119));
#20471=CARTESIAN_POINT('Ctrl Pts',(118.93791973272,5.50120927375035,332.816089809523));
#20472=CARTESIAN_POINT('Ctrl Pts',(118.945320599245,5.55741994889959,332.963385667914));
#20473=CARTESIAN_POINT('Ctrl Pts',(118.952721465771,5.60763888939149,333.112589962757));
#20474=CARTESIAN_POINT('Ctrl Pts',(118.960130459156,5.6579129750812,333.261958098181));
#20475=CARTESIAN_POINT('Ctrl Pts',(118.967539452541,5.70218206738238,333.413238501247));
#20476=CARTESIAN_POINT('Ctrl Pts',(118.974948445925,5.74032252734205,333.565905217711));
#20477=CARTESIAN_POINT('Ctrl Pts',(118.982362003506,5.77848648314067,333.718665982138));
#20478=CARTESIAN_POINT('Ctrl Pts',(118.989775561086,5.81051420777265,333.87281439715));
#20479=CARTESIAN_POINT('Ctrl Pts',(118.997189118666,5.83633353357012,334.027816145256));
#20480=CARTESIAN_POINT('Ctrl Pts',(119.004613230803,5.86218961790471,334.183038566727));
#20481=CARTESIAN_POINT('Ctrl Pts',(119.012037342939,5.88181960412198,334.339116378348));
#20482=CARTESIAN_POINT('Ctrl Pts',(119.019461455076,5.8952032692673,334.495511173047));
#20483=CARTESIAN_POINT('Ctrl Pts',(119.023318580231,5.90215662214518,334.576764565448));
#20484=CARTESIAN_POINT('Ctrl Pts',(119.027175705385,5.90742481412969,334.658103523739));
#20485=CARTESIAN_POINT('Ctrl Pts',(119.03103283054,5.91101055252681,334.73945286335));
#20486=CARTESIAN_POINT('Ctrl Pts',(119.038456807978,5.91791218000646,334.896029494305));
#20487=CARTESIAN_POINT('Ctrl Pts',(119.045880785416,5.91859859009121,335.053116743783));
#20488=CARTESIAN_POINT('Ctrl Pts',(119.053304762854,5.91301571514873,335.21018019627));
#20489=CARTESIAN_POINT('Ctrl Pts',(119.060719978881,5.90743942883867,335.367058290252));
#20490=CARTESIAN_POINT('Ctrl Pts',(119.068135194909,5.89560859785933,335.523912273796));
#20491=CARTESIAN_POINT('Ctrl Pts',(119.075550410936,5.87752100436485,335.680203944233));
#20492=CARTESIAN_POINT('Ctrl Pts',(119.082958492081,5.85945081466177,335.836345231612));
#20493=CARTESIAN_POINT('Ctrl Pts',(119.090366573225,5.83513589020854,335.991924914765));
#20494=CARTESIAN_POINT('Ctrl Pts',(119.097774654369,5.80462602573991,336.146406238557));
#20495=CARTESIAN_POINT('Ctrl Pts',(119.105177221543,5.77413887032061,336.300772579079));
#20496=CARTESIAN_POINT('Ctrl Pts',(119.112579788717,5.73746602807457,336.45404182349));
#20497=CARTESIAN_POINT('Ctrl Pts',(119.119982355891,5.69470893128614,336.6056838887));
#20498=CARTESIAN_POINT('Ctrl Pts',(119.127381025646,5.65197434592228,336.757246115025));
#20499=CARTESIAN_POINT('Ctrl Pts',(119.1347796954,5.60316198667137,336.907182510024));
#20500=CARTESIAN_POINT('Ctrl Pts',(119.142178365155,5.54842401457511,337.054974821497));
#20501=CARTESIAN_POINT('Ctrl Pts',(119.149575814359,5.49369507254455,337.202742751828));
#20502=CARTESIAN_POINT('Ctrl Pts',(119.156973263563,5.4330425872697,337.34836695099));
#20503=CARTESIAN_POINT('Ctrl Pts',(119.164370712767,5.36666810613794,337.49134582125));
#20504=CARTESIAN_POINT('Ctrl Pts',(119.17176784123,5.300296502888,337.634318492197));
#20505=CARTESIAN_POINT('Ctrl Pts',(119.179164969694,5.22820355422409,337.774645723783));
#20506=CARTESIAN_POINT('Ctrl Pts',(119.186562098157,5.1506382255489,337.911847597663));
#20507=CARTESIAN_POINT('Ctrl Pts',(119.193960365594,5.07306095374933,338.049070597206));
#20508=CARTESIAN_POINT('Ctrl Pts',(119.201358633031,4.99000980787323,338.18316695595));
#20509=CARTESIAN_POINT('Ctrl Pts',(119.208756900467,4.90177873629108,338.313683114443));
#20510=CARTESIAN_POINT('Ctrl Pts',(119.216157766993,4.81351666820564,338.444245124635));
#20511=CARTESIAN_POINT('Ctrl Pts',(119.223558633519,4.72007126015613,338.571224121381));
#20512=CARTESIAN_POINT('Ctrl Pts',(119.230959500045,4.62177853575142,338.694197305095));
#20513=CARTESIAN_POINT('Ctrl Pts',(119.238368493429,4.52337787653811,338.817305525121));
#20514=CARTESIAN_POINT('Ctrl Pts',(119.245777486814,4.42011950417836,338.936398855843));
#20515=CARTESIAN_POINT('Ctrl Pts',(119.253186480199,4.31237879668635,339.051088702607));
#20516=CARTESIAN_POINT('Ctrl Pts',(119.260600037779,4.20457171720212,339.165849202273));
#20517=CARTESIAN_POINT('Ctrl Pts',(119.268013595359,4.09227706595556,339.276200551594));
#20518=CARTESIAN_POINT('Ctrl Pts',(119.27542715294,3.9759051078579,339.381792913387));
#20519=CARTESIAN_POINT('Ctrl Pts',(119.282851265076,3.85936747297324,339.487535605238));
#20520=CARTESIAN_POINT('Ctrl Pts',(119.290275377213,3.73874122331871,339.588505539046));
#20521=CARTESIAN_POINT('Ctrl Pts',(119.29769948935,3.6144681730844,339.684394345938));
#20522=CARTESIAN_POINT('Ctrl Pts',(119.301556614504,3.54990332017233,339.734212441666));
#20523=CARTESIAN_POINT('Ctrl Pts',(119.305413739659,3.48435457582328,339.78265975426));
#20524=CARTESIAN_POINT('Ctrl Pts',(119.309270864814,3.41788662942578,339.829697873666));
#20525=CARTESIAN_POINT('Ctrl Pts',(119.316694842252,3.28995286668404,339.920234198828));
#20526=CARTESIAN_POINT('Ctrl Pts',(119.32411881969,3.15822630317177,340.00582034007));
#20527=CARTESIAN_POINT('Ctrl Pts',(119.331542797128,3.02312708119711,340.086121627865));
#20528=CARTESIAN_POINT('Ctrl Pts',(119.338958013155,2.88818729663119,340.166328148058));
#20529=CARTESIAN_POINT('Ctrl Pts',(119.346373229183,2.74988309404062,340.241262040663));
#20530=CARTESIAN_POINT('Ctrl Pts',(119.353788445211,2.60866585932778,340.310630188299));
#20531=CARTESIAN_POINT('Ctrl Pts',(119.361196526355,2.46758450312711,340.379931590253));
#20532=CARTESIAN_POINT('Ctrl Pts',(119.368604607499,2.32359602760543,340.443677745259));
#20533=CARTESIAN_POINT('Ctrl Pts',(119.376012688643,2.17717874839424,340.501620057768));
#20534=CARTESIAN_POINT('Ctrl Pts',(119.383415255817,2.03087045023813,340.559519242757));
#20535=CARTESIAN_POINT('Ctrl Pts',(119.390817822991,1.88213729353113,340.611623050069));
#20536=CARTESIAN_POINT('Ctrl Pts',(119.398220390165,1.73147992728075,340.657729917902));
#20537=CARTESIAN_POINT('Ctrl Pts',(119.40561905992,1.58090188147526,340.703812510671));
#20538=CARTESIAN_POINT('Ctrl Pts',(119.413017729674,1.42840199972534,340.743904343093));
#20539=CARTESIAN_POINT('Ctrl Pts',(119.420416399429,1.2744984344318,340.777852914633));
#20540=CARTESIAN_POINT('Ctrl Pts',(119.427813848633,1.12062025844746,340.811795885713));
#20541=CARTESIAN_POINT('Ctrl Pts',(119.435211297837,0.965339222595319,340.839597526962));
#20542=CARTESIAN_POINT('Ctrl Pts',(119.442608747041,0.809186199965505,340.861155880565));
#20543=CARTESIAN_POINT('Ctrl Pts',(119.450005875504,0.653039947858573,340.882713299436));
#20544=CARTESIAN_POINT('Ctrl Pts',(119.457403003968,0.496022153852965,340.898027917855));
#20545=CARTESIAN_POINT('Ctrl Pts',(119.464800132431,0.338671120990257,340.907049384787));
#20546=CARTESIAN_POINT('Ctrl Pts',(119.472198399868,0.181295859996387,340.916072240799));
#20547=CARTESIAN_POINT('Ctrl Pts',(119.479596667304,0.0235876306015942,
340.918799994577));
#20548=CARTESIAN_POINT('Ctrl Pts',(119.486994934741,-0.133913087046379,
340.915234386533));
#20549=CARTESIAN_POINT('Ctrl Pts',(119.494395801267,-0.291469136352832,
340.911667525853));
#20550=CARTESIAN_POINT('Ctrl Pts',(119.501796667793,-0.448817155885963,
340.901802909846));
#20551=CARTESIAN_POINT('Ctrl Pts',(119.509197534318,-0.605419762799319,
340.885694306818));
#20552=CARTESIAN_POINT('Ctrl Pts',(119.516606527703,-0.762194334346921,
340.869568015004));
#20553=CARTESIAN_POINT('Ctrl Pts',(119.524015521088,-0.918221487144169,
340.847184081594));
#20554=CARTESIAN_POINT('Ctrl Pts',(119.531424514473,-1.07297130507276,340.818647879103));
#20555=CARTESIAN_POINT('Ctrl Pts',(119.538838072053,-1.22781645422714,340.790094097327));
#20556=CARTESIAN_POINT('Ctrl Pts',(119.546251629633,-1.38138233736974,340.75538057647));
#20557=CARTESIAN_POINT('Ctrl Pts',(119.553665187213,-1.53315275106377,340.714663000073));
#20558=CARTESIAN_POINT('Ctrl Pts',(119.56108929935,-1.68513923772676,340.673887454753));
#20559=CARTESIAN_POINT('Ctrl Pts',(119.568513411487,-1.83532479438577,340.627090892807));
#20560=CARTESIAN_POINT('Ctrl Pts',(119.575937523623,-1.98321101606706,340.574477969124));
#20561=CARTESIAN_POINT('Ctrl Pts',(119.579794648778,-2.06004386223038,340.547143437039));
#20562=CARTESIAN_POINT('Ctrl Pts',(119.583651773933,-2.13625642772459,340.518239720244));
#20563=CARTESIAN_POINT('Ctrl Pts',(119.587508899088,-2.21178140557564,340.487800431544));
#20564=CARTESIAN_POINT('Ctrl Pts',(119.594932876526,-2.35714763277035,340.429212601625));
#20565=CARTESIAN_POINT('Ctrl Pts',(119.602356853964,-2.50040364682574,340.364756496062));
#20566=CARTESIAN_POINT('Ctrl Pts',(119.609780831402,-2.64104065388809,340.294604312601));
#20567=CARTESIAN_POINT('Ctrl Pts',(119.617196047429,-2.78151168812214,340.224534919271));
#20568=CARTESIAN_POINT('Ctrl Pts',(119.624611263457,-2.91936953697372,340.148782993716));
#20569=CARTESIAN_POINT('Ctrl Pts',(119.632026479485,-3.05412344097235,340.067569493337));
#20570=CARTESIAN_POINT('Ctrl Pts',(119.639434560629,-3.18874768544304,339.98643413618));
#20571=CARTESIAN_POINT('Ctrl Pts',(119.646842641773,-3.32027361331372,339.899847857481));
#20572=CARTESIAN_POINT('Ctrl Pts',(119.654250722917,-3.44823333125121,339.808078353745));
#20573=CARTESIAN_POINT('Ctrl Pts',(119.661653290091,-3.57609780643372,339.716377155726));
#20574=CARTESIAN_POINT('Ctrl Pts',(119.669055857265,-3.70040105498996,339.61950063102));
#20575=CARTESIAN_POINT('Ctrl Pts',(119.676458424439,-3.82070264939387,339.517760709402));
#20576=CARTESIAN_POINT('Ctrl Pts',(119.683857094194,-3.9409409055341,339.416074353407));
#20577=CARTESIAN_POINT('Ctrl Pts',(119.691255763949,-4.05718141919617,339.309529940394));
#20578=CARTESIAN_POINT('Ctrl Pts',(119.698654433703,-4.16901554743048,339.198480668978));
#20579=CARTESIAN_POINT('Ctrl Pts',(119.706051882907,-4.28083122650625,339.087449717244));
#20580=CARTESIAN_POINT('Ctrl Pts',(119.713449332111,-4.38824169827882,338.971915644758));
#20581=CARTESIAN_POINT('Ctrl Pts',(119.720846781315,-4.49087393835445,338.852269698802));
#20582=CARTESIAN_POINT('Ctrl Pts',(119.728243909779,-4.59350172847507,338.732628940486));
#20583=CARTESIAN_POINT('Ctrl Pts',(119.735641038242,-4.69135145584257,338.608876946457));
#20584=CARTESIAN_POINT('Ctrl Pts',(119.743038166706,-4.7840894725324,338.481439139394));
#20585=CARTESIAN_POINT('Ctrl Pts',(119.750436434142,-4.87684176856185,338.353981710089));
#20586=CARTESIAN_POINT('Ctrl Pts',(119.757834701579,-4.96448056712965,338.222837639521));
#20587=CARTESIAN_POINT('Ctrl Pts',(119.765232969016,-5.04671484696492,338.088462370812));
#20588=CARTESIAN_POINT('Ctrl Pts',(119.772633835541,-5.12897801656741,337.954039894659));
#20589=CARTESIAN_POINT('Ctrl Pts',(119.780034702067,-5.20583269251164,337.816384278407));
#20590=CARTESIAN_POINT('Ctrl Pts',(119.787435568593,-5.27703328101997,337.675976515874));
#20591=CARTESIAN_POINT('Ctrl Pts',(119.794844561978,-5.3483120545816,337.535414572193));
#20592=CARTESIAN_POINT('Ctrl Pts',(119.802253555362,-5.41392417265137,337.392094779954));
#20593=CARTESIAN_POINT('Ctrl Pts',(119.809662548747,-5.47367147720706,337.24651978004));
#20594=CARTESIAN_POINT('Ctrl Pts',(119.817076106328,-5.5334555881633,337.100855100904));
#20595=CARTESIAN_POINT('Ctrl Pts',(119.824489663908,-5.58736755887069,336.952932795587));
#20596=CARTESIAN_POINT('Ctrl Pts',(119.831903221488,-5.63525895964167,336.803271199869));
#20597=CARTESIAN_POINT('Ctrl Pts',(119.839327333625,-5.68321854258926,336.653396533471));
#20598=CARTESIAN_POINT('Ctrl Pts',(119.846751445761,-5.72514033764196,336.501777989953));
#20599=CARTESIAN_POINT('Ctrl Pts',(119.854175557898,-5.76092672793034,336.348945439192));
#20600=CARTESIAN_POINT('Ctrl Pts',(119.858032683053,-5.77951919846822,336.269542775936));
#20601=CARTESIAN_POINT('Ctrl Pts',(119.861889808207,-5.79645643864578,336.189812544041));
#20602=CARTESIAN_POINT('Ctrl Pts',(119.865746933362,-5.81173029052009,336.109829533195));
#20603=CARTESIAN_POINT('Ctrl Pts',(119.876717981006,-5.85517460459028,335.882329157253));
#20604=CARTESIAN_POINT('Ctrl Pts',(119.88768902865,-5.88527075000024,335.652204915708));
#20605=CARTESIAN_POINT('Ctrl Pts',(119.898660076294,-5.90177227769661,335.420730964765));
#20606=CARTESIAN_POINT('Ctrl Pts',(119.905207257627,-5.91161987818216,335.282594482274));
#20607=CARTESIAN_POINT('Ctrl Pts',(119.911754438961,-5.91662676190817,335.143977687089));
#20608=CARTESIAN_POINT('Ctrl Pts',(119.918301620294,-5.91674775276501,335.005156806208));
#20609=CARTESIAN_POINT('',(121.668301620294,-5.90704278596851,335.000701560224));
#20610=CARTESIAN_POINT('Ctrl Pts',(119.918302821709,-5.91937129153481,335.005133607679));
#20611=CARTESIAN_POINT('Ctrl Pts',(119.993530203684,-5.9047448003301,333.409354599871));
#20612=CARTESIAN_POINT('Ctrl Pts',(120.161503597084,-4.41496513658335,329.822132368592));
#20613=CARTESIAN_POINT('Ctrl Pts',(120.42222300191,1.6527734744595,328.201399940917));
#20614=CARTESIAN_POINT('Ctrl Pts',(120.700461036183,6.6114983946026,332.710739879489));
#20615=CARTESIAN_POINT('Ctrl Pts',(120.978699070458,5.50294882358002,339.320900041228));
#20616=CARTESIAN_POINT('Ctrl Pts',(121.256937104732,-0.655575659453675,
341.965834011514));
#20617=CARTESIAN_POINT('Ctrl Pts',(121.486804621343,-5.24644207849654,338.869813694043));
#20618=CARTESIAN_POINT('Ctrl Pts',(121.623926126531,-5.90804155338697,335.94701070509));
#20619=CARTESIAN_POINT('Ctrl Pts',(121.668301620294,-5.90704278596851,335.000701560224));
#20620=CARTESIAN_POINT('',(123.418301620294,-5.91678917890862,334.994557826597));
#20621=CARTESIAN_POINT('Ctrl Pts',(121.668301620294,-5.90704278596851,335.000701560224));
#20622=CARTESIAN_POINT('Ctrl Pts',(121.716672137956,-5.90595410181071,333.96919837404));
#20623=CARTESIAN_POINT('Ctrl Pts',(121.85778866704,-5.15714314318895,330.95840379715));
#20624=CARTESIAN_POINT('Ctrl Pts',(122.091651207554,-0.355313788212134,
328.012412788873));
#20625=CARTESIAN_POINT('Ctrl Pts',(122.369889241826,5.68373048077245,330.919824667594));
#20626=CARTESIAN_POINT('Ctrl Pts',(122.648127276101,6.50689917927394,337.571553225575));
#20627=CARTESIAN_POINT('Ctrl Pts',(122.926365310375,1.35878254263427,341.86340534451));
#20628=CARTESIAN_POINT('Ctrl Pts',(123.183090091772,-4.5418059823907,340.011960697189));
#20629=CARTESIAN_POINT('Ctrl Pts',(123.347068861746,-5.90282340540148,336.507293395397));
#20630=CARTESIAN_POINT('Ctrl Pts',(123.418301620294,-5.91678917890862,334.994557826597));
#20631=CARTESIAN_POINT('',(125.168301620294,-5.92166611962084,335.002060437347));
#20632=CARTESIAN_POINT('Ctrl Pts',(123.418301620294,-5.91678917890862,334.994557826597));
#20633=CARTESIAN_POINT('Ctrl Pts',(123.43981487317,-5.92100703068346,334.537691302128));
#20634=CARTESIAN_POINT('Ctrl Pts',(123.554074137475,-5.66376034564121,332.115921753525));
#20635=CARTESIAN_POINT('Ctrl Pts',(123.761079413193,-2.33387325834533,328.404118062362));
#20636=CARTESIAN_POINT('Ctrl Pts',(124.039317447472,4.28362510061816,329.467985997979));
#20637=CARTESIAN_POINT('Ctrl Pts',(124.317555481744,6.97010393094322,335.608501530848));
#20638=CARTESIAN_POINT('Ctrl Pts',(124.595793516019,3.2602212624124,341.190604190331));
#20639=CARTESIAN_POINT('Ctrl Pts',(124.874031550292,-3.44151833785114,341.091680757513));
#20640=CARTESIAN_POINT('Ctrl Pts',(125.064867585051,-5.8719165109706,337.189631756557));
#20641=CARTESIAN_POINT('Ctrl Pts',(125.162957608385,-5.92613979826577,335.115110298055));
#20642=CARTESIAN_POINT('Ctrl Pts',(125.168301620294,-5.92563084334104,335.002061816868));
#20643=CARTESIAN_POINT('',(126.918301605958,-5.91317602257575,335.004338125692));
#20644=CARTESIAN_POINT('Ctrl Pts',(125.168301620294,-5.91674964183415,335.002058726664));
#20645=CARTESIAN_POINT('Ctrl Pts',(125.175660465658,-5.91680372602739,334.846621564152));
#20646=CARTESIAN_POINT('Ctrl Pts',(125.183019311023,-5.91072843215637,334.690935239553));
#20647=CARTESIAN_POINT('Ctrl Pts',(125.190378156387,-5.89849104658582,334.535528326109));
#20648=CARTESIAN_POINT('Ctrl Pts',(125.197728580823,-5.88626766459175,334.380299249066));
#20649=CARTESIAN_POINT('Ctrl Pts',(125.205079005259,-5.86789625240156,334.225349322313));
#20650=CARTESIAN_POINT('Ctrl Pts',(125.212429429694,-5.84339606690749,334.071208867533));
#20651=CARTESIAN_POINT('Ctrl Pts',(125.219773114474,-5.81891834580424,333.917209745209));
#20652=CARTESIAN_POINT('Ctrl Pts',(125.227116799254,-5.78832309503642,333.764018990799));
#20653=CARTESIAN_POINT('Ctrl Pts',(125.234460484035,-5.7516814910038,333.612163342268));
#20654=CARTESIAN_POINT('Ctrl Pts',(125.241799104385,-5.71506515614384,333.460412418044));
#20655=CARTESIAN_POINT('Ctrl Pts',(125.249137724735,-5.67241085738215,333.309995135077));
#20656=CARTESIAN_POINT('Ctrl Pts',(125.256476345085,-5.62384108261946,333.161429348667));
#20657=CARTESIAN_POINT('Ctrl Pts',(125.263812275111,-5.57528911344133,333.012918026185));
#20658=CARTESIAN_POINT('Ctrl Pts',(125.271148205138,-5.52082609893917,332.866257211193));
#20659=CARTESIAN_POINT('Ctrl Pts',(125.278484135164,-5.46062473218843,332.721950813369));
#20660=CARTESIAN_POINT('Ctrl Pts',(125.285818790569,-5.40043382545311,332.577669488847));
#20661=CARTESIAN_POINT('Ctrl Pts',(125.293153445974,-5.33450669609768,332.435742118593));
#20662=CARTESIAN_POINT('Ctrl Pts',(125.300488101379,-5.26306455513068,332.296653545876));
#20663=CARTESIAN_POINT('Ctrl Pts',(125.307822991486,-5.19162012807683,332.157560522443));
#20664=CARTESIAN_POINT('Ctrl Pts',(125.315157881594,-5.1146605117602,332.021306815763));
#20665=CARTESIAN_POINT('Ctrl Pts',(125.322492771702,-5.03245322137383,331.888353307783));
#20666=CARTESIAN_POINT('Ctrl Pts',(125.329829405769,-4.95022638519947,331.755368188481));
#20667=CARTESIAN_POINT('Ctrl Pts',(125.337166039837,-4.8627495918676,331.625685152828));
#20668=CARTESIAN_POINT('Ctrl Pts',(125.344502673904,-4.77033394129497,331.499736488344));
#20669=CARTESIAN_POINT('Ctrl Pts',(125.351846889461,-4.67782279076226,331.373657671745));
#20670=CARTESIAN_POINT('Ctrl Pts',(125.359191105017,-4.58036281404226,331.251321241386));
#20671=CARTESIAN_POINT('Ctrl Pts',(125.366535320574,-4.47830613495872,331.13312726818));
#20672=CARTESIAN_POINT('Ctrl Pts',(125.373883425499,-4.37619540844046,331.014870701511));
#20673=CARTESIAN_POINT('Ctrl Pts',(125.381231530424,-4.26948338942717,330.900761239732));
#20674=CARTESIAN_POINT('Ctrl Pts',(125.388579635349,-4.1585589029352,330.791161868957));
#20675=CARTESIAN_POINT('Ctrl Pts',(125.395938932375,-4.04746546430145,330.681395564361));
#20676=CARTESIAN_POINT('Ctrl Pts',(125.403298229401,-3.93214702006758,330.576153331447));
#20677=CARTESIAN_POINT('Ctrl Pts',(125.410657526427,-3.81302603730524,330.475758295434));
#20678=CARTESIAN_POINT('Ctrl Pts',(125.417274223898,-3.7059251141289,330.385493752698));
#20679=CARTESIAN_POINT('Ctrl Pts',(125.423890921369,-3.59575091723202,330.299147088162));
#20680=CARTESIAN_POINT('Ctrl Pts',(125.43050761884,-3.48282925362775,330.216922439206));
#20681=CARTESIAN_POINT('Ctrl Pts',(125.437931596278,-3.35613041534751,330.124665850272));
#20682=CARTESIAN_POINT('Ctrl Pts',(125.445355573716,-3.22557223999351,330.037307748441));
#20683=CARTESIAN_POINT('Ctrl Pts',(125.452779551154,-3.09157030976495,329.95518844928));
#20684=CARTESIAN_POINT('Ctrl Pts',(125.460194767182,-2.95772652197589,329.873166063247));
#20685=CARTESIAN_POINT('Ctrl Pts',(125.46760998321,-2.82044738418279,329.79637036648));
#20686=CARTESIAN_POINT('Ctrl Pts',(125.475025199237,-2.68018028074308,329.725100548331));
#20687=CARTESIAN_POINT('Ctrl Pts',(125.482433280381,-2.54004814160414,329.653899305642));
#20688=CARTESIAN_POINT('Ctrl Pts',(125.489841361525,-2.39693409092009,329.588213524397));
#20689=CARTESIAN_POINT('Ctrl Pts',(125.497249442669,-2.25131304185891,329.52829824003));
#20690=CARTESIAN_POINT('Ctrl Pts',(125.504652009843,-2.10580038120366,329.468427551703));
#20691=CARTESIAN_POINT('Ctrl Pts',(125.512054577017,-1.95778478131893,329.41431894951));
#20692=CARTESIAN_POINT('Ctrl Pts',(125.519457144191,-1.80776412218853,329.366180741182));
#20693=CARTESIAN_POINT('Ctrl Pts',(125.526855813946,-1.65782244827945,329.31806787741));
#20694=CARTESIAN_POINT('Ctrl Pts',(125.534254483701,-1.50587817199397,329.275919261005));
#20695=CARTESIAN_POINT('Ctrl Pts',(125.541653153456,-1.35244733798393,329.239894379399));
#20696=CARTESIAN_POINT('Ctrl Pts',(125.54905060266,-1.19904181529744,329.20387544078));
#20697=CARTESIAN_POINT('Ctrl Pts',(125.556448051864,-1.04415058457771,329.173978317212));
#20698=CARTESIAN_POINT('Ctrl Pts',(125.563845501068,-0.888303092893294,
329.150312129895));
#20699=CARTESIAN_POINT('Ctrl Pts',(125.571242629531,-0.732462358484304,
329.126646968702));
#20700=CARTESIAN_POINT('Ctrl Pts',(125.578639757995,-0.575665814531576,
329.109212262618));
#20701=CARTESIAN_POINT('Ctrl Pts',(125.586036886458,-0.418451034642092,
329.098065631159));
#20702=CARTESIAN_POINT('Ctrl Pts',(125.593435153895,-0.261212047601114,
329.086917283397));
#20703=CARTESIAN_POINT('Ctrl Pts',(125.600833421331,-0.103555068698107,
329.082058964482));
#20704=CARTESIAN_POINT('Ctrl Pts',(125.608231688768,0.0539794477389267,
329.083496236651));
#20705=CARTESIAN_POINT('Ctrl Pts',(125.615632555294,0.211569307707187,329.084934013749));
#20706=CARTESIAN_POINT('Ctrl Pts',(125.623033421819,0.36903624659141,329.092671782033));
#20707=CARTESIAN_POINT('Ctrl Pts',(125.630434288345,0.525842204127269,329.106663038748));
#20708=CARTESIAN_POINT('Ctrl Pts',(125.63784328173,0.682820349596862,329.1206696592));
#20709=CARTESIAN_POINT('Ctrl Pts',(125.645252275115,0.839135692259169,329.140943448517));
#20710=CARTESIAN_POINT('Ctrl Pts',(125.652661268499,0.994256940666024,329.167386203559));
#20711=CARTESIAN_POINT('Ctrl Pts',(125.66007482608,1.14947374911271,329.19384524825));
#20712=CARTESIAN_POINT('Ctrl Pts',(125.66748838366,1.30349463326513,329.226480754076));
#20713=CARTESIAN_POINT('Ctrl Pts',(125.67490194124,1.45580133334682,329.265144026192));
#20714=CARTESIAN_POINT('Ctrl Pts',(125.682326053377,1.60832486989955,329.303862342553));
#20715=CARTESIAN_POINT('Ctrl Pts',(125.689750165513,1.75912899148776,329.348625458518));
#20716=CARTESIAN_POINT('Ctrl Pts',(125.69717427765,1.90771257351594,329.399235471889));
#20717=CARTESIAN_POINT('Ctrl Pts',(125.701031402805,1.98490772645645,329.425529411429));
#20718=CARTESIAN_POINT('Ctrl Pts',(125.70488852796,2.06150385678267,329.453400773127));
#20719=CARTESIAN_POINT('Ctrl Pts',(125.708745653115,2.13743320951783,329.482816856642));
#20720=CARTESIAN_POINT('Ctrl Pts',(125.716169630553,2.28357775473181,329.5394352788));
#20721=CARTESIAN_POINT('Ctrl Pts',(125.723593607991,2.42769156637605,329.601949952284));
#20722=CARTESIAN_POINT('Ctrl Pts',(125.731017585429,2.5692635704555,329.670195569439));
#20723=CARTESIAN_POINT('Ctrl Pts',(125.738432801456,2.71066849826958,329.738360646497));
#20724=CARTESIAN_POINT('Ctrl Pts',(125.745848017484,2.8495372565809,329.812243044133));
#20725=CARTESIAN_POINT('Ctrl Pts',(125.753263233512,2.98537614533413,329.891628455822));
#20726=CARTESIAN_POINT('Ctrl Pts',(125.760671314656,3.12108433059251,329.970937483267));
#20727=CARTESIAN_POINT('Ctrl Pts',(125.7680793958,3.25376813009427,330.055738796411));
#20728=CARTESIAN_POINT('Ctrl Pts',(125.775487476944,3.3829560763368,330.145771044947));
#20729=CARTESIAN_POINT('Ctrl Pts',(125.782890044118,3.51204786563145,330.235736280836));
#20730=CARTESIAN_POINT('Ctrl Pts',(125.790292611292,3.63764867780338,330.330924487156));
#20731=CARTESIAN_POINT('Ctrl Pts',(125.797695178466,3.75931391100921,330.431029713273));
#20732=CARTESIAN_POINT('Ctrl Pts',(125.805093848221,3.88091508800178,330.531082234427));
#20733=CARTESIAN_POINT('Ctrl Pts',(125.812492517976,3.99858452519743,330.636046383121));
#20734=CARTESIAN_POINT('Ctrl Pts',(125.81989118773,4.1119088448398,330.7455745142));
#20735=CARTESIAN_POINT('Ctrl Pts',(125.827288636934,4.2252144694881,330.855084576537));
#20736=CARTESIAN_POINT('Ctrl Pts',(125.834686086138,4.33417613112258,330.969156867851));
#20737=CARTESIAN_POINT('Ctrl Pts',(125.842083535342,4.43841555321163,331.087405216546));
#20738=CARTESIAN_POINT('Ctrl Pts',(125.849480663806,4.54265045566111,331.2056484382));
#20739=CARTESIAN_POINT('Ctrl Pts',(125.856877792269,4.64216327887674,331.328067077253));
#20740=CARTESIAN_POINT('Ctrl Pts',(125.864274920733,4.73661465745414,331.454240257816));
#20741=CARTESIAN_POINT('Ctrl Pts',(125.871673188169,4.83108057918615,331.5804328659));
#20742=CARTESIAN_POINT('Ctrl Pts',(125.879071455606,4.92048328084934,331.71038086779));
#20743=CARTESIAN_POINT('Ctrl Pts',(125.886469723043,5.00452561419233,331.843632793956));
#20744=CARTESIAN_POINT('Ctrl Pts',(125.893870589569,5.08859747249114,331.976931532925));
#20745=CARTESIAN_POINT('Ctrl Pts',(125.901271456094,5.16730501414479,332.113536191656));
#20746=CARTESIAN_POINT('Ctrl Pts',(125.90867232262,5.24039616903024,332.252969138485));
#20747=CARTESIAN_POINT('Ctrl Pts',(125.916081316005,5.31356758499118,332.39255519602));
#20748=CARTESIAN_POINT('Ctrl Pts',(125.92349030939,5.38111012431931,332.534975413216));
#20749=CARTESIAN_POINT('Ctrl Pts',(125.930899302774,5.44281885584106,332.679729872407));
#20750=CARTESIAN_POINT('Ctrl Pts',(125.938312860355,5.50456560207012,332.824573505338));
#20751=CARTESIAN_POINT('Ctrl Pts',(125.945726417935,5.5604712471035,332.971753897542));
#20752=CARTESIAN_POINT('Ctrl Pts',(125.953139975515,5.61038037150751,333.120754766002));
#20753=CARTESIAN_POINT('Ctrl Pts',(125.960564087652,5.66036055068711,333.269967764477));
#20754=CARTESIAN_POINT('Ctrl Pts',(125.967988199788,5.70432705482221,333.421006058142));
#20755=CARTESIAN_POINT('Ctrl Pts',(125.975412311925,5.74217511682058,333.573341144398));
#20756=CARTESIAN_POINT('Ctrl Pts',(125.97926943708,5.76183870881543,333.652485354815));
#20757=CARTESIAN_POINT('Ctrl Pts',(125.983126562234,5.77985164735605,333.731979467978));
#20758=CARTESIAN_POINT('Ctrl Pts',(125.986983687388,5.79620476475206,333.81174881125));
#20759=CARTESIAN_POINT('Ctrl Pts',(125.994407664826,5.82768032484627,333.965284354171));
#20760=CARTESIAN_POINT('Ctrl Pts',(126.001831642264,5.85309865495061,334.120303009829));
#20761=CARTESIAN_POINT('Ctrl Pts',(126.009255619702,5.87232219433602,334.276285547741));
#20762=CARTESIAN_POINT('Ctrl Pts',(126.01667083573,5.89152304705262,334.432084002789));
#20763=CARTESIAN_POINT('Ctrl Pts',(126.024086051758,5.90454361607854,334.58884370902));
#20764=CARTESIAN_POINT('Ctrl Pts',(126.031501267785,5.91129694691432,334.746033529966));
#20765=CARTESIAN_POINT('Ctrl Pts',(126.038909348929,5.91804377972916,334.903072103658));
#20766=CARTESIAN_POINT('Ctrl Pts',(126.046317430073,5.91853536365466,335.060539597784));
#20767=CARTESIAN_POINT('Ctrl Pts',(126.053725511217,5.91273633562185,335.217898113615));
#20768=CARTESIAN_POINT('Ctrl Pts',(126.061128078391,5.90694162391154,335.375139504628));
#20769=CARTESIAN_POINT('Ctrl Pts',(126.068530645565,5.89486563690517,335.532271707497));
#20770=CARTESIAN_POINT('Ctrl Pts',(126.075933212739,5.87652505544912,335.688755279601));
#20771=CARTESIAN_POINT('Ctrl Pts',(126.083331882494,5.858194130229,335.84515646379));
#20772=CARTESIAN_POINT('Ctrl Pts',(126.090730552249,5.83360522261793,336.000909327594));
#20773=CARTESIAN_POINT('Ctrl Pts',(126.098129222003,5.80282697242064,336.155478122098));
#20774=CARTESIAN_POINT('Ctrl Pts',(126.105526671207,5.77205379967888,336.310021417551));
#20775=CARTESIAN_POINT('Ctrl Pts',(126.112924120411,5.73509338361726,336.463380665711));
#20776=CARTESIAN_POINT('Ctrl Pts',(126.120321569615,5.69206575703082,336.615028786164));
#20777=CARTESIAN_POINT('Ctrl Pts',(126.127718698079,5.64903999604724,336.766670331418));
#20778=CARTESIAN_POINT('Ctrl Pts',(126.135115826542,5.59994764946738,336.916600537445));
#20779=CARTESIAN_POINT('Ctrl Pts',(126.142512955006,5.54495899071204,337.064306264541));
#20780=CARTESIAN_POINT('Ctrl Pts',(126.149911222442,5.48996186507595,337.212034734631));
#20781=CARTESIAN_POINT('Ctrl Pts',(126.157309489879,5.42906674976437,337.35753769402));
#20782=CARTESIAN_POINT('Ctrl Pts',(126.164707757315,5.36249249116697,337.500320948334));
#20783=CARTESIAN_POINT('Ctrl Pts',(126.172108623841,5.29589484433234,337.643154363907));
#20784=CARTESIAN_POINT('Ctrl Pts',(126.179509490367,5.22361423949961,337.783265834048));
#20785=CARTESIAN_POINT('Ctrl Pts',(126.186910356893,5.14591591771836,337.920184913712));
#20786=CARTESIAN_POINT('Ctrl Pts',(126.194319350277,5.06813227575147,338.057254343616));
#20787=CARTESIAN_POINT('Ctrl Pts',(126.201728343662,4.9849192203301,338.191124057489));
#20788=CARTESIAN_POINT('Ctrl Pts',(126.209137337047,4.8965862428685,338.321351190201));
#20789=CARTESIAN_POINT('Ctrl Pts',(126.216550894627,4.80819884924603,338.451658547319));
#20790=CARTESIAN_POINT('Ctrl Pts',(126.223964452207,4.7146854698793,338.578318552352));
#20791=CARTESIAN_POINT('Ctrl Pts',(126.231378009788,4.61639615179771,338.70092111942));
#20792=CARTESIAN_POINT('Ctrl Pts',(126.238802121924,4.51796690087738,338.823698233687));
#20793=CARTESIAN_POINT('Ctrl Pts',(126.246226234061,4.41474837565924,338.942406092276));
#20794=CARTESIAN_POINT('Ctrl Pts',(126.253650346198,4.30712830976852,339.056670591223));
#20795=CARTESIAN_POINT('Ctrl Pts',(126.257507471352,4.25121535268365,339.116035598789));
#20796=CARTESIAN_POINT('Ctrl Pts',(126.261364596507,4.19411489161567,339.174201889104));
#20797=CARTESIAN_POINT('Ctrl Pts',(126.265221721662,4.13588475921477,339.231121343213));
#20798=CARTESIAN_POINT('Ctrl Pts',(126.2726456991,4.02380667726986,339.34067670534));
#20799=CARTESIAN_POINT('Ctrl Pts',(126.280069676538,3.9072034994721,339.445941010946));
#20800=CARTESIAN_POINT('Ctrl Pts',(126.287493653976,3.78643741580906,339.546517596871));
#20801=CARTESIAN_POINT('Ctrl Pts',(126.294908870003,3.6658138542949,339.646975487293));
#20802=CARTESIAN_POINT('Ctrl Pts',(126.302324086031,3.54103745002422,339.74275643348));
#20803=CARTESIAN_POINT('Ctrl Pts',(126.309739302058,3.41250779091417,339.833499885119));
#20804=CARTESIAN_POINT('Ctrl Pts',(126.317147383202,3.28410180239487,339.924156023867));
#20805=CARTESIAN_POINT('Ctrl Pts',(126.324555464347,3.15195005143188,340.009784103832));
#20806=CARTESIAN_POINT('Ctrl Pts',(126.331963545491,3.01648573155637,340.090063299588));
#20807=CARTESIAN_POINT('Ctrl Pts',(126.339366112665,2.88112224024904,340.170282742073));
#20808=CARTESIAN_POINT('Ctrl Pts',(126.346768679839,2.74245140909999,340.245161038185));
#20809=CARTESIAN_POINT('Ctrl Pts',(126.354171247013,2.60093589387887,340.314420291851));
#20810=CARTESIAN_POINT('Ctrl Pts',(126.361569916767,2.45949488595717,340.383643080822));
#20811=CARTESIAN_POINT('Ctrl Pts',(126.368968586522,2.31521251112293,340.447252555533));
#20812=CARTESIAN_POINT('Ctrl Pts',(126.376367256277,2.1685764370063,340.505016512179));
#20813=CARTESIAN_POINT('Ctrl Pts',(126.383764705481,2.02196455328866,340.562770939565));
#20814=CARTESIAN_POINT('Ctrl Pts',(126.391162154685,1.87300008781617,340.614681626114));
#20815=CARTESIAN_POINT('Ctrl Pts',(126.398559603889,1.72219123038617,340.660564276508));
#20816=CARTESIAN_POINT('Ctrl Pts',(126.405956732352,1.57138891176553,340.70644493751));
#20817=CARTESIAN_POINT('Ctrl Pts',(126.413353860816,1.4187427172452,340.746297973406));
#20818=CARTESIAN_POINT('Ctrl Pts',(126.420750989279,1.26477630166613,340.779988881412));
#20819=CARTESIAN_POINT('Ctrl Pts',(126.428149256716,1.11078617910208,340.813684976976));
#20820=CARTESIAN_POINT('Ctrl Pts',(126.435547524152,0.95547579532685,340.841216975654));
#20821=CARTESIAN_POINT('Ctrl Pts',(126.442945791589,0.799379159269492,340.862501473111));
#20822=CARTESIAN_POINT('Ctrl Pts',(126.450346658115,0.64322768482256,340.883793448036));
#20823=CARTESIAN_POINT('Ctrl Pts',(126.45774752464,0.486289777699041,340.898833501481));
#20824=CARTESIAN_POINT('Ctrl Pts',(126.465148391166,0.329104582324897,340.907590095495));
#20825=CARTESIAN_POINT('Ctrl Pts',(126.472557384551,0.171746782578905,340.916356305087));
#20826=CARTESIAN_POINT('Ctrl Pts',(126.479966377936,0.0141415251459065,
340.91882525513));
#20827=CARTESIAN_POINT('Ctrl Pts',(126.48737537132,-0.143171291674783,340.915017543824));
#20828=CARTESIAN_POINT('Ctrl Pts',(126.494788928901,-0.300581018617045,
340.911207486835));
#20829=CARTESIAN_POINT('Ctrl Pts',(126.502202486481,-0.457697574394116,
340.901113087579));
#20830=CARTESIAN_POINT('Ctrl Pts',(126.509616044061,-0.613986678505744,
340.884806787068));
#20831=CARTESIAN_POINT('Ctrl Pts',(126.517040156198,-0.7704982887694,340.868477271552));
#20832=CARTESIAN_POINT('Ctrl Pts',(126.524464268334,-0.926179726250687,
340.845918245364));
#20833=CARTESIAN_POINT('Ctrl Pts',(126.531888380471,-1.08050657403185,340.817253312859));
#20834=CARTESIAN_POINT('Ctrl Pts',(126.535745505626,-1.1606855847594,340.802360726353));
#20835=CARTESIAN_POINT('Ctrl Pts',(126.539602630781,-1.24049919512095,340.785820847726));
#20836=CARTESIAN_POINT('Ctrl Pts',(126.543459755936,-1.3198756442952,340.76765626976));
#20837=CARTESIAN_POINT('Ctrl Pts',(126.550883733374,-1.4726549667486,340.732694112303));
#20838=CARTESIAN_POINT('Ctrl Pts',(126.558307710812,-1.624274637244,340.691604568301));
#20839=CARTESIAN_POINT('Ctrl Pts',(126.56573168825,-1.77420509148286,340.644477553845));
#20840=CARTESIAN_POINT('Ctrl Pts',(126.573146904277,-1.92395860522736,340.597406156356));
#20841=CARTESIAN_POINT('Ctrl Pts',(126.580562120305,-2.07202651829239,340.544311581908));
#20842=CARTESIAN_POINT('Ctrl Pts',(126.587977336333,-2.21788939627793,340.485334738043));
#20843=CARTESIAN_POINT('Ctrl Pts',(126.595385417477,-2.36361192573639,340.4264146414));
#20844=CARTESIAN_POINT('Ctrl Pts',(126.602793498621,-2.50713330028566,340.361623682088));
#20845=CARTESIAN_POINT('Ctrl Pts',(126.610201579765,-2.6479493051041,340.291152524743));
#20846=CARTESIAN_POINT('Ctrl Pts',(126.617604146939,-2.7886604979979,340.220733820368));
#20847=CARTESIAN_POINT('Ctrl Pts',(126.625006714113,-2.9266699983226,340.144643502584));
#20848=CARTESIAN_POINT('Ctrl Pts',(126.632409281287,-3.06149374775632,340.063120242987));
#20849=CARTESIAN_POINT('Ctrl Pts',(126.639807951042,-3.19624651307612,339.98163990503));
#20850=CARTESIAN_POINT('Ctrl Pts',(126.647206620796,-3.32781654935287,339.894732514579));
#20851=CARTESIAN_POINT('Ctrl Pts',(126.654605290551,-3.45574468651726,339.802682502946));
#20852=CARTESIAN_POINT('Ctrl Pts',(126.662002739755,-3.58365171951144,339.710647676708));
#20853=CARTESIAN_POINT('Ctrl Pts',(126.669400188959,-3.70791774314308,339.6134721308));
#20854=CARTESIAN_POINT('Ctrl Pts',(126.676797638163,-3.82811276888865,339.511483480095));
#20855=CARTESIAN_POINT('Ctrl Pts',(126.684194766626,-3.94830258318694,339.409499251441));
#20856=CARTESIAN_POINT('Ctrl Pts',(126.69159189509,-4.06442146599077,339.302702574395));
#20857=CARTESIAN_POINT('Ctrl Pts',(126.698989023553,-4.17607293135745,339.19146101431));
#20858=CARTESIAN_POINT('Ctrl Pts',(126.70638729099,-4.28774158826329,339.080202325802));
#20859=CARTESIAN_POINT('Ctrl Pts',(126.713785558427,-4.39494119368948,338.964497654954));
#20860=CARTESIAN_POINT('Ctrl Pts',(126.721183825863,-4.49731262827982,338.844750926395));
#20861=CARTESIAN_POINT('Ctrl Pts',(126.728584692389,-4.59972002703177,338.724962129551));
#20862=CARTESIAN_POINT('Ctrl Pts',(126.735985558915,-4.6972956354792,338.601128731244));
#20863=CARTESIAN_POINT('Ctrl Pts',(126.743386425441,-4.78972117070168,338.473687042529));
#20864=CARTESIAN_POINT('Ctrl Pts',(126.750795418825,-4.88224819799774,338.346105410656));
#20865=CARTESIAN_POINT('Ctrl Pts',(126.75820441221,-4.96961363894644,338.214907877856));
#20866=CARTESIAN_POINT('Ctrl Pts',(126.765613405595,-5.05154264506381,338.080559602995));
#20867=CARTESIAN_POINT('Ctrl Pts',(126.773026963175,-5.13352212227506,337.946128564962));
#20868=CARTESIAN_POINT('Ctrl Pts',(126.780440520755,-5.21005831026275,337.808543242619));
#20869=CARTESIAN_POINT('Ctrl Pts',(126.787854078336,-5.28092299638487,337.668292125828));
#20870=CARTESIAN_POINT('Ctrl Pts',(126.795278190472,-5.35188857136094,337.527841335895));
#20871=CARTESIAN_POINT('Ctrl Pts',(126.802702302609,-5.41716636378353,337.384717510292));
#20872=CARTESIAN_POINT('Ctrl Pts',(126.810126414746,-5.47657652310742,337.239428531802));
#20873=CARTESIAN_POINT('Ctrl Pts',(126.8139835399,-5.5074424927685,337.163945058046));
#20874=CARTESIAN_POINT('Ctrl Pts',(126.817840665055,-5.53672548023707,337.087877412965));
#20875=CARTESIAN_POINT('Ctrl Pts',(126.82169779021,-5.56440565036725,337.011298168015));
#20876=CARTESIAN_POINT('Ctrl Pts',(126.830305803929,-5.62617997053476,336.840394926689));
#20877=CARTESIAN_POINT('Ctrl Pts',(126.838913817648,-5.68012201448321,336.666518829418));
#20878=CARTESIAN_POINT('Ctrl Pts',(126.847521831367,-5.7259766090411,336.490343059572));
#20879=CARTESIAN_POINT('Ctrl Pts',(126.856096835013,-5.77165536006907,336.314842889838));
#20880=CARTESIAN_POINT('Ctrl Pts',(126.864671838659,-5.80930848155199,336.137060763736));
#20881=CARTESIAN_POINT('Ctrl Pts',(126.873246842305,-5.83873032688343,335.957684046245));
#20882=CARTESIAN_POINT('Ctrl Pts',(126.88175746393,-5.86793126993042,335.779654107863));
#20883=CARTESIAN_POINT('Ctrl Pts',(126.890268085554,-5.88902400299891,335.60005356052));
#20884=CARTESIAN_POINT('Ctrl Pts',(126.898778707178,-5.90185462755575,335.419574210002));
#20885=CARTESIAN_POINT('Ctrl Pts',(126.90528633359,-5.9116655338497,335.281571107497));
#20886=CARTESIAN_POINT('Ctrl Pts',(126.911793960003,-5.91664663233737,335.143054595291));
#20887=CARTESIAN_POINT('Ctrl Pts',(126.918301586416,-5.91674840742824,335.004341162903));
#20888=CARTESIAN_POINT('',(128.668301620294,-5.90987324019195,334.996005152984));
#20889=CARTESIAN_POINT('Ctrl Pts',(126.918301620294,-5.91055548896683,335.004335897736));
#20890=CARTESIAN_POINT('Ctrl Pts',(126.978846355024,-5.90182962359021,333.715137151976));
#20891=CARTESIAN_POINT('Ctrl Pts',(127.132137101179,-4.85228408488346,330.438137618077));
#20892=CARTESIAN_POINT('Ctrl Pts',(127.378173858758,0.561399630138656,328.025944266319));
#20893=CARTESIAN_POINT('Ctrl Pts',(127.656411893032,6.16843780437573,331.698031197188));
#20894=CARTESIAN_POINT('Ctrl Pts',(127.934649927306,6.11479165153577,338.400286161418));
#20895=CARTESIAN_POINT('Ctrl Pts',(128.21288796158,0.449691454254745,341.982148703458));
#20896=CARTESIAN_POINT('Ctrl Pts',(128.457438525909,-4.89222166567316,339.498698145784));
#20897=CARTESIAN_POINT('Ctrl Pts',(128.609243078814,-5.90208820652118,336.253922582036));
#20898=CARTESIAN_POINT('Ctrl Pts',(128.668301620294,-5.90987324019195,334.996005152984));
#20899=CARTESIAN_POINT('',(130.418301620294,-5.92512223992695,334.997412588165));
#20900=CARTESIAN_POINT('Ctrl Pts',(128.668301620294,-5.90987324019195,334.996005152984));
#20901=CARTESIAN_POINT('Ctrl Pts',(128.701989090239,-5.91431388639194,334.278478872759));
#20902=CARTESIAN_POINT('Ctrl Pts',(128.828422571606,-5.46072358895401,331.590931601405));
#20903=CARTESIAN_POINT('Ctrl Pts',(129.047602064403,-1.45139077720003,328.155579810305));
#20904=CARTESIAN_POINT('Ctrl Pts',(129.325840098675,4.97018812648249,330.075586033998));
#20905=CARTESIAN_POINT('Ctrl Pts',(129.60407813295,6.83069874635309,336.514654270055));
#20906=CARTESIAN_POINT('Ctrl Pts',(129.882316167224,2.42277794764036,341.563746638746));
#20907=CARTESIAN_POINT('Ctrl Pts',(130.153723996339,-4.04570561128838,340.613304275294));
#20908=CARTESIAN_POINT('Ctrl Pts',(130.332385814028,-5.91517505445709,336.815309996308));
#20909=CARTESIAN_POINT('Ctrl Pts',(130.418301620294,-5.92512223992695,334.997412588165));
#20910=CARTESIAN_POINT('',(132.168301620294,-5.91772602350224,335.005383180983));
#20911=CARTESIAN_POINT('Ctrl Pts',(130.418301620294,-5.92512223992695,334.997412588165));
#20912=CARTESIAN_POINT('Ctrl Pts',(130.425131825453,-5.92591302942736,334.852891890574));
#20913=CARTESIAN_POINT('Ctrl Pts',(130.431962030612,-5.92108494976179,334.708424922706));
#20914=CARTESIAN_POINT('Ctrl Pts',(130.531538247196,-5.76631470651247,332.608488631998));
#20915=CARTESIAN_POINT('Ctrl Pts',(130.717030270046,-3.34356564080936,328.854010110094));
#20916=CARTESIAN_POINT('Ctrl Pts',(130.995268304318,3.35889879536448,328.862376534545));
#20917=CARTESIAN_POINT('Ctrl Pts',(131.273506338593,6.9789513843005,334.503149422067));
#20918=CARTESIAN_POINT('Ctrl Pts',(131.551744372867,4.19452329701571,340.599874751459));
#20919=CARTESIAN_POINT('Ctrl Pts',(131.829982407141,-2.43915690887765,341.557677675449));
#20920=CARTESIAN_POINT('Ctrl Pts',(132.035501489616,-5.68572389466333,337.82007499618));
#20921=CARTESIAN_POINT('Ctrl Pts',(132.148274560668,-5.92169754062293,335.430510874451));
#20922=CARTESIAN_POINT('Ctrl Pts',(132.168301620294,-5.91775274132979,335.005383205287));
#20923=CARTESIAN_POINT('',(133.918301620327,-5.91674999725183,334.999819665701));
#20924=CARTESIAN_POINT('Ctrl Pts',(132.168301620294,-5.91674755194479,335.005382290896));
#20925=CARTESIAN_POINT('Ctrl Pts',(132.175608191324,-5.91688861786857,334.850308647478));
#20926=CARTESIAN_POINT('Ctrl Pts',(132.182914762354,-5.91092897118882,334.695048870305));
#20927=CARTESIAN_POINT('Ctrl Pts',(132.190221333384,-5.89885154245384,334.54012931971));
#20928=CARTESIAN_POINT('Ctrl Pts',(132.197522434716,-5.88678315488013,334.385325741867));
#20929=CARTESIAN_POINT('Ctrl Pts',(132.204823536047,-5.86860612946989,334.230862265239));
#20930=CARTESIAN_POINT('Ctrl Pts',(132.212124637379,-5.84435546471036,334.077265062648));
#20931=CARTESIAN_POINT('Ctrl Pts',(132.219422532179,-5.82011545047365,333.92373531761));
#20932=CARTESIAN_POINT('Ctrl Pts',(132.226720426978,-5.78980716211582,333.771071468783));
#20933=CARTESIAN_POINT('Ctrl Pts',(132.234018321778,-5.7535174123303,333.619794236894));
#20934=CARTESIAN_POINT('Ctrl Pts',(132.241314622808,-5.71723558777236,333.46855004206));
#20935=CARTESIAN_POINT('Ctrl Pts',(132.248610923838,-5.67497498934015,333.318692235538));
#20936=CARTESIAN_POINT('Ctrl Pts',(132.255907224869,-5.62687342336098,333.170730736066));
#20937=CARTESIAN_POINT('Ctrl Pts',(132.263203465538,-5.57877225532201,333.022770460667));
#20938=CARTESIAN_POINT('Ctrl Pts',(132.270499706206,-5.52483033456661,332.87670682684));
#20939=CARTESIAN_POINT('Ctrl Pts',(132.277795946875,-5.46523506958358,332.733033701906));
#20940=CARTESIAN_POINT('Ctrl Pts',(132.285093660387,-5.40562777450211,332.589331574637));
#20941=CARTESIAN_POINT('Ctrl Pts',(132.292391373899,-5.34036501207566,332.448021271395));
#20942=CARTESIAN_POINT('Ctrl Pts',(132.299689087412,-5.26968184756498,332.309575537588));
#20943=CARTESIAN_POINT('Ctrl Pts',(132.306994129754,-5.19892769849957,332.17099076772));
#20944=CARTESIAN_POINT('Ctrl Pts',(132.314299172097,-5.12274244955002,332.035276656283));
#20945=CARTESIAN_POINT('Ctrl Pts',(132.32160421444,-5.04140685708058,331.902880779841));
#20946=CARTESIAN_POINT('Ctrl Pts',(132.328912947963,-4.96003016638047,331.77041800481));
#20947=CARTESIAN_POINT('Ctrl Pts',(132.336221681486,-4.87349816264455,331.641277123254));
#20948=CARTESIAN_POINT('Ctrl Pts',(132.343530415009,-4.78213378647513,331.515875000699));
#20949=CARTESIAN_POINT('Ctrl Pts',(132.350850335794,-4.69062956156016,331.390280928828));
#20950=CARTESIAN_POINT('Ctrl Pts',(132.358170256578,-4.59427842480844,331.268437350721));
#20951=CARTESIAN_POINT('Ctrl Pts',(132.365490177363,-4.49344291375054,331.150727166936));
#20952=CARTESIAN_POINT('Ctrl Pts',(132.372479610139,-4.39716003766225,331.038331494808));
#20953=CARTESIAN_POINT('Ctrl Pts',(132.379469042914,-4.2967890634065,330.929704339512));
#20954=CARTESIAN_POINT('Ctrl Pts',(132.386458475689,-4.19267440833758,330.825145287777));
#20955=CARTESIAN_POINT('Ctrl Pts',(132.393882453127,-4.08208677196621,330.71408562586));
#20956=CARTESIAN_POINT('Ctrl Pts',(132.401306430565,-3.96691647582864,330.607255489685));
#20957=CARTESIAN_POINT('Ctrl Pts',(132.408730408003,-3.84752031749017,330.505056399798));
#20958=CARTESIAN_POINT('Ctrl Pts',(132.416145624031,-3.72826506458258,330.402977920213));
#20959=CARTESIAN_POINT('Ctrl Pts',(132.423560840059,-3.60479415725262,330.305519848415));
#20960=CARTESIAN_POINT('Ctrl Pts',(132.430976056086,-3.47750227550635,330.213048100686));
#20961=CARTESIAN_POINT('Ctrl Pts',(132.43838413723,-3.35033287336785,330.120665328806));
#20962=CARTESIAN_POINT('Ctrl Pts',(132.445792218375,-3.21935011601256,330.033259547323));
#20963=CARTESIAN_POINT('Ctrl Pts',(132.453200299519,-3.0849828227206,329.951157405304));
#20964=CARTESIAN_POINT('Ctrl Pts',(132.460602866693,-2.95071554145869,329.869116373408));
#20965=CARTESIAN_POINT('Ctrl Pts',(132.468005433867,-2.81306905740038,329.792371314498));
#20966=CARTESIAN_POINT('Ctrl Pts',(132.475408001041,-2.6725022293984,329.721206350277));
#20967=CARTESIAN_POINT('Ctrl Pts',(132.482806670795,-2.53200940921738,329.650078854098));
#20968=CARTESIAN_POINT('Ctrl Pts',(132.49020534055,-2.38859963934369,329.584525769764));
#20969=CARTESIAN_POINT('Ctrl Pts',(132.497604010305,-2.24275740556107,329.524785868817));
#20970=CARTESIAN_POINT('Ctrl Pts',(132.505001459509,-2.09693923121828,329.465055823099));
#20971=CARTESIAN_POINT('Ctrl Pts',(132.512398908713,-1.94868973440439,329.411137198802));
#20972=CARTESIAN_POINT('Ctrl Pts',(132.519796357917,-1.79851456849425,329.363221140632));
#20973=CARTESIAN_POINT('Ctrl Pts',(132.52719348638,-1.64834591391749,329.315307160019));
#20974=CARTESIAN_POINT('Ctrl Pts',(132.534590614844,-1.4962521118089,329.273395341495));
#20975=CARTESIAN_POINT('Ctrl Pts',(132.541987743307,-1.3427549519279,329.237627250726));
#20976=CARTESIAN_POINT('Ctrl Pts',(132.549386010744,-1.18923415731613,329.201853652565));
#20977=CARTESIAN_POINT('Ctrl Pts',(132.55678427818,-1.03430993817985,329.172225750434));
#20978=CARTESIAN_POINT('Ctrl Pts',(132.564182545617,-0.87851512781858,329.148834156111));
#20979=CARTESIAN_POINT('Ctrl Pts',(132.571583412143,-0.722665585101663,
329.125434344075));
#20980=CARTESIAN_POINT('Ctrl Pts',(132.578984278668,-0.565945211059111,
329.108275257264));
#20981=CARTESIAN_POINT('Ctrl Pts',(132.586385145194,-0.408892674791273,
329.097395715195));
#20982=CARTESIAN_POINT('Ctrl Pts',(132.593794138579,-0.251667679824081,
329.086504226348));
#20983=CARTESIAN_POINT('Ctrl Pts',(132.601203131964,-0.0941101667556998,
329.081906078811));
#20984=CARTESIAN_POINT('Ctrl Pts',(132.608612125348,0.0632397370914502,
329.083587970894));
#20985=CARTESIAN_POINT('Ctrl Pts',(132.616025682928,0.220686573906835,329.08527089908));
#20986=CARTESIAN_POINT('Ctrl Pts',(132.623439240509,0.377925174792565,329.093241556974));
#20987=CARTESIAN_POINT('Ctrl Pts',(132.630852798089,0.534420329258209,329.1074347289));
#20988=CARTESIAN_POINT('Ctrl Pts',(132.638276910226,0.691138283226448,329.121648107404));
#20989=CARTESIAN_POINT('Ctrl Pts',(132.645701022362,0.847110307828953,329.142101644517));
#20990=CARTESIAN_POINT('Ctrl Pts',(132.653125134499,1.0018103639836,329.168678832622));
#20991=CARTESIAN_POINT('Ctrl Pts',(132.656982259653,1.08218327147926,329.182486751857));
#20992=CARTESIAN_POINT('Ctrl Pts',(132.660839384808,1.16221306871678,329.197946749815));
#20993=CARTESIAN_POINT('Ctrl Pts',(132.664696509963,1.2418276961715,329.215037205347));
#20994=CARTESIAN_POINT('Ctrl Pts',(132.6721204874,1.39506545078927,329.24793195239));
#20995=CARTESIAN_POINT('Ctrl Pts',(132.679544464838,1.54722644712942,329.286969194867));
#20996=CARTESIAN_POINT('Ctrl Pts',(132.686968442276,1.69777995436494,329.332066179898));
#20997=CARTESIAN_POINT('Ctrl Pts',(132.694383658304,1.84815578580951,329.377109943702));
#20998=CARTESIAN_POINT('Ctrl Pts',(132.701798874332,1.99692755027547,329.428199109019));
#20999=CARTESIAN_POINT('Ctrl Pts',(132.709214090359,2.14357395695826,329.485199799308));
#21000=CARTESIAN_POINT('Ctrl Pts',(132.716622171503,2.29007926120713,329.54214564382));
#21001=CARTESIAN_POINT('Ctrl Pts',(132.724030252647,2.43446293337107,329.604991555171));
#21002=CARTESIAN_POINT('Ctrl Pts',(132.731438333792,2.57621822856086,329.673553698634));
#21003=CARTESIAN_POINT('Ctrl Pts',(132.738840900966,2.71786801269573,329.742064810042));
#21004=CARTESIAN_POINT('Ctrl Pts',(132.74624346814,2.85689298069465,329.816283520038));
#21005=CARTESIAN_POINT('Ctrl Pts',(132.753646035314,2.99280589370071,329.895977718982));
#21006=CARTESIAN_POINT('Ctrl Pts',(132.761044705068,3.12864724915136,329.975629959277));
#21007=CARTESIAN_POINT('Ctrl Pts',(132.768443374823,3.26137949161004,330.060751758909));
#21008=CARTESIAN_POINT('Ctrl Pts',(132.775842044578,3.39053964993582,330.151064916426));
#21009=CARTESIAN_POINT('Ctrl Pts',(132.783239493782,3.51967850084685,330.241363175078));
#21010=CARTESIAN_POINT('Ctrl Pts',(132.790636942986,3.64524613160197,330.336850878255));
#21011=CARTESIAN_POINT('Ctrl Pts',(132.79803439219,3.76680816648433,330.437206250617));
#21012=CARTESIAN_POINT('Ctrl Pts',(132.805431520653,3.88836493064862,330.537557271745));
#21013=CARTESIAN_POINT('Ctrl Pts',(132.812828649117,4.00591615645688,330.642775304813));
#21014=CARTESIAN_POINT('Ctrl Pts',(132.82022577758,4.11906042793937,330.752498174988));
#21015=CARTESIAN_POINT('Ctrl Pts',(132.827624045017,4.23222212081522,330.862237939745));
#21016=CARTESIAN_POINT('Ctrl Pts',(132.835022312454,4.34097524032482,330.976483662888));
#21017=CARTESIAN_POINT('Ctrl Pts',(132.84242057989,4.44495524241974,331.094836308759));
#21018=CARTESIAN_POINT('Ctrl Pts',(132.849821446416,4.5489717737832,331.21323053316));
#21019=CARTESIAN_POINT('Ctrl Pts',(132.857222312942,4.64821160296261,331.335734272713));
#21020=CARTESIAN_POINT('Ctrl Pts',(132.864623179468,4.74235058104108,331.461915556548));
#21021=CARTESIAN_POINT('Ctrl Pts',(132.872032172852,4.83659293271748,331.588235399495));
#21022=CARTESIAN_POINT('Ctrl Pts',(132.879441166237,4.92572302404798,331.718240552102));
#21023=CARTESIAN_POINT('Ctrl Pts',(132.886850159622,5.00945974682138,331.851469611473));
#21024=CARTESIAN_POINT('Ctrl Pts',(132.894263717202,5.09324805430448,331.98478074454));
#21025=CARTESIAN_POINT('Ctrl Pts',(132.901677274782,5.17163618732362,332.121319418906));
#21026=CARTESIAN_POINT('Ctrl Pts',(132.909090832363,5.24438935402489,332.260600272707));
#21027=CARTESIAN_POINT('Ctrl Pts',(132.916514944499,5.31724609817802,332.400079418302));
#21028=CARTESIAN_POINT('Ctrl Pts',(132.923939056636,5.38445169464843,332.542308203863));
#21029=CARTESIAN_POINT('Ctrl Pts',(132.931363168773,5.44581944724451,332.686781222946));
#21030=CARTESIAN_POINT('Ctrl Pts',(132.935220293928,5.47770246542406,332.761840772939));
#21031=CARTESIAN_POINT('Ctrl Pts',(132.939077419082,5.50801053871094,332.837505828788));
#21032=CARTESIAN_POINT('Ctrl Pts',(132.942934544237,5.53672285324849,332.913704093659));
#21033=CARTESIAN_POINT('Ctrl Pts',(132.950358521675,5.59198670048542,333.060366225826));
#21034=CARTESIAN_POINT('Ctrl Pts',(132.957782499113,5.64150249657939,333.209446945721));
#21035=CARTESIAN_POINT('Ctrl Pts',(132.965206476551,5.68505262128808,333.360455168138));
#21036=CARTESIAN_POINT('Ctrl Pts',(132.972621692578,5.72855135029715,333.511285178132));
#21037=CARTESIAN_POINT('Ctrl Pts',(132.980036908606,5.76609831951695,333.664037807627));
#21038=CARTESIAN_POINT('Ctrl Pts',(132.987452124634,5.79752400822152,333.818202243785));
#21039=CARTESIAN_POINT('Ctrl Pts',(132.994860205778,5.82891945928666,333.972218343699));
#21040=CARTESIAN_POINT('Ctrl Pts',(133.002268286922,5.85420528141425,334.127643182641));
#21041=CARTESIAN_POINT('Ctrl Pts',(133.009676368066,5.87326183641131,334.283951144506));
#21042=CARTESIAN_POINT('Ctrl Pts',(133.01707893524,5.89230420726639,334.440142763499));
#21043=CARTESIAN_POINT('Ctrl Pts',(133.024481502414,5.90512649807899,334.597215827704));
#21044=CARTESIAN_POINT('Ctrl Pts',(133.031884069588,5.91166022189539,334.754634999725));
#21045=CARTESIAN_POINT('Ctrl Pts',(133.039282739343,5.91819050573482,334.911971291242));
#21046=CARTESIAN_POINT('Ctrl Pts',(133.046681409097,5.91843880099984,335.069652955714));
#21047=CARTESIAN_POINT('Ctrl Pts',(133.054080078852,5.91238851297488,335.227140120064));
#21048=CARTESIAN_POINT('Ctrl Pts',(133.061477528056,5.90633922305962,335.384601303921));
#21049=CARTESIAN_POINT('Ctrl Pts',(133.06887497726,5.89399342638746,335.541867678763));
#21050=CARTESIAN_POINT('Ctrl Pts',(133.076272426464,5.87538664508347,335.698399837682));
#21051=CARTESIAN_POINT('Ctrl Pts',(133.083669554928,5.85678067053709,335.85492520964));
#21052=CARTESIAN_POINT('Ctrl Pts',(133.091066683391,5.83191429517451,336.01071605837));
#21053=CARTESIAN_POINT('Ctrl Pts',(133.098463811854,5.80087485032623,336.165238831035));
#21054=CARTESIAN_POINT('Ctrl Pts',(133.105862079291,5.76983062617831,336.31978539635));
#21055=CARTESIAN_POINT('Ctrl Pts',(133.113260346728,5.73261151348119,336.473063130902));
#21056=CARTESIAN_POINT('Ctrl Pts',(133.120658614164,5.68935579413008,336.624549540734));
#21057=CARTESIAN_POINT('Ctrl Pts',(133.12805948069,5.64608487858958,336.776089169335));
#21058=CARTESIAN_POINT('Ctrl Pts',(133.135460347216,5.59677323644561,336.925835861617));
#21059=CARTESIAN_POINT('Ctrl Pts',(133.142861213742,5.54160870564134,337.073283269614));
#21060=CARTESIAN_POINT('Ctrl Pts',(133.150270207126,5.4863835989086,337.22089258896));
#21061=CARTESIAN_POINT('Ctrl Pts',(133.157679200511,5.42529289924552,337.366197232037));
#21062=CARTESIAN_POINT('Ctrl Pts',(133.165088193896,5.35857248640835,337.508711117368));
#21063=CARTESIAN_POINT('Ctrl Pts',(133.172501751476,5.29181097149536,337.651312796169));
#21064=CARTESIAN_POINT('Ctrl Pts',(133.179915309056,5.21941300398327,337.791119960849));
#21065=CARTESIAN_POINT('Ctrl Pts',(133.187328866636,5.1416596756735,337.927672512774));
#21066=CARTESIAN_POINT('Ctrl Pts',(133.194752978773,5.06379565126632,338.064419472256));
#21067=CARTESIAN_POINT('Ctrl Pts',(133.20217709091,4.98056123567708,338.197902249049));
#21068=CARTESIAN_POINT('Ctrl Pts',(133.209601203046,4.89228040394408,338.327690341917));
#21069=CARTESIAN_POINT('Ctrl Pts',(133.213458328201,4.84641495761344,338.395120481517));
#21070=CARTESIAN_POINT('Ctrl Pts',(133.217315453356,4.7991880354374,338.46155389032));
#21071=CARTESIAN_POINT('Ctrl Pts',(133.221172578511,4.75064916979636,338.526933941544));
#21072=CARTESIAN_POINT('Ctrl Pts',(133.228596555949,4.65722429273634,338.652773784875));
#21073=CARTESIAN_POINT('Ctrl Pts',(133.236020533387,4.55865497336079,338.775088805969));
#21074=CARTESIAN_POINT('Ctrl Pts',(133.243444510825,4.45523640889637,338.893430248938));
#21075=CARTESIAN_POINT('Ctrl Pts',(133.250859726852,4.35193989389799,339.011632031199));
#21076=CARTESIAN_POINT('Ctrl Pts',(133.25827494288,4.24380576841043,339.125869291409));
#21077=CARTESIAN_POINT('Ctrl Pts',(133.265690158908,4.13117184845439,339.235723045837));
#21078=CARTESIAN_POINT('Ctrl Pts',(133.273098240052,4.01864630428893,339.345471099536));
#21079=CARTESIAN_POINT('Ctrl Pts',(133.280506321196,3.90162985063131,339.45084378544));
#21080=CARTESIAN_POINT('Ctrl Pts',(133.28791440234,3.78049974618856,339.551456056205));
#21081=CARTESIAN_POINT('Ctrl Pts',(133.295316969514,3.65945980109538,339.651993439419));
#21082=CARTESIAN_POINT('Ctrl Pts',(133.302719536688,3.5343125876999,339.747777225207));
#21083=CARTESIAN_POINT('Ctrl Pts',(133.310122103862,3.40547122041814,339.838460119646));
#21084=CARTESIAN_POINT('Ctrl Pts',(133.317520773617,3.27669768755225,339.929095269938));
#21085=CARTESIAN_POINT('Ctrl Pts',(133.324919443371,3.14423417872232,340.014634663141));
#21086=CARTESIAN_POINT('Ctrl Pts',(133.332318113126,3.00852570436372,340.094772188104));
#21087=CARTESIAN_POINT('Ctrl Pts',(133.33971556233,2.87283961769004,340.174896492864));
#21088=CARTESIAN_POINT('Ctrl Pts',(133.347113011534,2.73390994897294,340.249620508427));
#21089=CARTESIAN_POINT('Ctrl Pts',(133.354510460738,2.59220952004958,340.318682202075));
#21090=CARTESIAN_POINT('Ctrl Pts',(133.361907589202,2.45051523500969,340.387740901328));
#21091=CARTESIAN_POINT('Ctrl Pts',(133.369304717665,2.30605076411907,340.451137603309));
#21092=CARTESIAN_POINT('Ctrl Pts',(133.376701846129,2.15931204333547,340.508657010743));
#21093=CARTESIAN_POINT('Ctrl Pts',(133.384100113565,2.0125507284519,340.566185274729));
#21094=CARTESIAN_POINT('Ctrl Pts',(133.391498381002,1.86351481391656,340.617834306068));
#21095=CARTESIAN_POINT('Ctrl Pts',(133.398896648439,1.71271850831408,340.663437637494));
#21096=CARTESIAN_POINT('Ctrl Pts',(133.406297514964,1.56186922638492,340.709056989849));
#21097=CARTESIAN_POINT('Ctrl Pts',(133.41369838149,1.40925867907596,340.748626305608));
#21098=CARTESIAN_POINT('Ctrl Pts',(133.421099248016,1.25541431508246,340.782029527768));
#21099=CARTESIAN_POINT('Ctrl Pts',(133.4285082414,1.10140101526794,340.81546942986));
#21100=CARTESIAN_POINT('Ctrl Pts',(133.435917234785,0.946151557994752,340.842729637148));
#21101=CARTESIAN_POINT('Ctrl Pts',(133.44332622817,0.790202347615889,340.863745459373));
#21102=CARTESIAN_POINT('Ctrl Pts',(133.45073978575,0.634157067144336,340.88477422807));
#21103=CARTESIAN_POINT('Ctrl Pts',(133.45815334333,0.477411545294794,340.899550911588));
#21104=CARTESIAN_POINT('Ctrl Pts',(133.465566900911,0.320504803726773,340.908062900248));
#21105=CARTESIAN_POINT('Ctrl Pts',(133.472991013047,0.163374676686341,340.916587007282));
#21106=CARTESIAN_POINT('Ctrl Pts',(133.480415125184,0.00608324368542446,
340.918828601248));
#21107=CARTESIAN_POINT('Ctrl Pts',(133.487839237321,-0.150832156118545,
340.914827150744));
#21108=CARTESIAN_POINT('Ctrl Pts',(133.491696362475,-0.232356023833892,
340.912748236107));
#21109=CARTESIAN_POINT('Ctrl Pts',(133.49555348763,-0.313778492059307,340.908985039158));
#21110=CARTESIAN_POINT('Ctrl Pts',(133.499410612785,-0.395025137311746,
340.903548568733));
#21111=CARTESIAN_POINT('Ctrl Pts',(133.506834590223,-0.551404107939601,
340.893084756396));
#21112=CARTESIAN_POINT('Ctrl Pts',(133.514258567661,-0.707602933274411,
340.876387389198));
#21113=CARTESIAN_POINT('Ctrl Pts',(133.521682545099,-0.86308449675833,340.853461857222));
#21114=CARTESIAN_POINT('Ctrl Pts',(133.529097761126,-1.01838256860399,340.830563380824));
#21115=CARTESIAN_POINT('Ctrl Pts',(133.536512977154,-1.17296469789577,340.801451424193));
#21116=CARTESIAN_POINT('Ctrl Pts',(133.543928193182,-1.32629574064238,340.766183327891));
#21117=CARTESIAN_POINT('Ctrl Pts',(133.551336274326,-1.47947924903135,340.730949166374));
#21118=CARTESIAN_POINT('Ctrl Pts',(133.55874435547,-1.63141370611187,340.689570740683));
#21119=CARTESIAN_POINT('Ctrl Pts',(133.566152436614,-1.78157116102391,340.642156924502));
#21120=CARTESIAN_POINT('Ctrl Pts',(133.573555003788,-1.9316168510008,340.59477839929));
#21121=CARTESIAN_POINT('Ctrl Pts',(133.580957570962,-2.07988781804193,340.541373540209));
#21122=CARTESIAN_POINT('Ctrl Pts',(133.588360138136,-2.22586845536354,340.482101803316));
#21123=CARTESIAN_POINT('Ctrl Pts',(133.595758807891,-2.37177223451766,340.422861272733));
#21124=CARTESIAN_POINT('Ctrl Pts',(133.603157477646,-2.51538774054721,340.357760156084));
#21125=CARTESIAN_POINT('Ctrl Pts',(133.6105561474,-2.65621673737412,340.287007017831));
#21126=CARTESIAN_POINT('Ctrl Pts',(133.617953596604,-2.79702250178873,340.216265551649));
#21127=CARTESIAN_POINT('Ctrl Pts',(133.625351045808,-2.93504233616722,340.139874081774));
#21128=CARTESIAN_POINT('Ctrl Pts',(133.632748495012,-3.06980002058145,340.058088413239));
#21129=CARTESIAN_POINT('Ctrl Pts',(133.640145623476,-3.20455186213775,339.976306290787));
#21130=CARTESIAN_POINT('Ctrl Pts',(133.647542751939,-3.33604151591193,339.889130628345));
#21131=CARTESIAN_POINT('Ctrl Pts',(133.654939880403,-3.46381955442744,339.79686195933));
#21132=CARTESIAN_POINT('Ctrl Pts',(133.662338147839,-3.59161726757216,339.704579083242));
#21133=CARTESIAN_POINT('Ctrl Pts',(133.669736415276,-3.71570192494373,339.607201857645));
#21134=CARTESIAN_POINT('Ctrl Pts',(133.677134682713,-3.83565527289649,339.505072606518));
#21135=CARTESIAN_POINT('Ctrl Pts',(133.684535549238,-3.9556507617203,339.402907476313));
#21136=CARTESIAN_POINT('Ctrl Pts',(133.691936415764,-4.07151176745755,339.295987238521));
#21137=CARTESIAN_POINT('Ctrl Pts',(133.69933728229,-4.18285526254338,339.184692630901));
#21138=CARTESIAN_POINT('Ctrl Pts',(133.706746275674,-4.29432102343238,339.07327581116));
#21139=CARTESIAN_POINT('Ctrl Pts',(133.714155269059,-4.40125910285416,338.95747529279));
#21140=CARTESIAN_POINT('Ctrl Pts',(133.721564262444,-4.50332482221643,338.837707142046));
#21141=CARTESIAN_POINT('Ctrl Pts',(133.728977820024,-4.60545341758201,338.71786520999));
#21142=CARTESIAN_POINT('Ctrl Pts',(133.736391377604,-4.70270344192746,338.594051067985));
#21143=CARTESIAN_POINT('Ctrl Pts',(133.743804935185,-4.79477259595615,338.466711167024));
#21144=CARTESIAN_POINT('Ctrl Pts',(133.751229047321,-4.88697282728141,338.339189974401));
#21145=CARTESIAN_POINT('Ctrl Pts',(133.758653159458,-4.97397725124649,338.208133307842));
#21146=CARTESIAN_POINT('Ctrl Pts',(133.766077271595,-5.05552827278849,338.074014386033));
#21147=CARTESIAN_POINT('Ctrl Pts',(133.769934396749,-5.09789731177662,338.004334206438));
#21148=CARTESIAN_POINT('Ctrl Pts',(133.773791521904,-5.13879512875485,337.933827834035));
#21149=CARTESIAN_POINT('Ctrl Pts',(133.777648647058,-5.17819070646937,337.862563810631));
#21150=CARTESIAN_POINT('Ctrl Pts',(133.785435791969,-5.25772638659632,337.71868896734));
#21151=CARTESIAN_POINT('Ctrl Pts',(133.79322293688,-5.331356706861,337.571325915128));
#21152=CARTESIAN_POINT('Ctrl Pts',(133.801010081791,-5.39877815383162,337.420976044535));
#21153=CARTESIAN_POINT('Ctrl Pts',(133.808784649618,-5.46609070785334,337.270869005288));
#21154=CARTESIAN_POINT('Ctrl Pts',(133.816559217445,-5.52721424522438,337.117785053094));
#21155=CARTESIAN_POINT('Ctrl Pts',(133.824333785272,-5.58189044811685,336.962251153069));
#21156=CARTESIAN_POINT('Ctrl Pts',(133.83216443819,-5.63696108062936,336.805595244312));
#21157=CARTESIAN_POINT('Ctrl Pts',(133.839995091109,-5.68549079118679,336.646454167424));
#21158=CARTESIAN_POINT('Ctrl Pts',(133.847825744027,-5.72726324714731,336.485390945299));
#21159=CARTESIAN_POINT('Ctrl Pts',(133.855573568673,-5.76859385739756,336.326031359987));
#21160=CARTESIAN_POINT('Ctrl Pts',(133.863321393318,-5.80330934948144,336.16479040582));
#21161=CARTESIAN_POINT('Ctrl Pts',(133.871069217963,-5.8312485558455,336.002232928241));
#21162=CARTESIAN_POINT('Ctrl Pts',(133.878941285018,-5.85963578917091,335.837068714744));
#21163=CARTESIAN_POINT('Ctrl Pts',(133.886813352073,-5.88102741061079,335.670545696006));
#21164=CARTESIAN_POINT('Ctrl Pts',(133.894685419128,-5.89530726613627,335.503272093743));
#21165=CARTESIAN_POINT('Ctrl Pts',(133.902557486184,-5.90958712166176,335.335998491481));
#21166=CARTESIAN_POINT('Ctrl Pts',(133.910429553239,-5.91675512236119,335.167974647051));
#21167=CARTESIAN_POINT('Ctrl Pts',(133.918301620294,-5.91674999725185,334.999819666414));
#21168=CARTESIAN_POINT('',(135.668301620294,-5.91694958252063,334.994690602227));
#21169=CARTESIAN_POINT('Ctrl Pts',(133.918301620327,-5.91674999725183,334.999819665701));
#21170=CARTESIAN_POINT('Ctrl Pts',(133.926068049142,-5.91674494089828,334.833921220247));
#21171=CARTESIAN_POINT('Ctrl Pts',(133.933834477957,-5.90975819896838,334.668163927719));
#21172=CARTESIAN_POINT('Ctrl Pts',(133.941600906772,-5.89585107127789,334.503139146429));
#21173=CARTESIAN_POINT('Ctrl Pts',(133.949377678458,-5.88192542289534,334.337894594872));
#21174=CARTESIAN_POINT('Ctrl Pts',(133.957154450145,-5.86106101844648,334.173384815219));
#21175=CARTESIAN_POINT('Ctrl Pts',(133.964931221831,-5.83337059116754,334.010192893235));
#21176=CARTESIAN_POINT('Ctrl Pts',(133.972726562797,-5.80561404502803,333.846611303594));
#21177=CARTESIAN_POINT('Ctrl Pts',(133.980521903763,-5.77099893364784,333.684354176176));
#21178=CARTESIAN_POINT('Ctrl Pts',(133.988317244729,-5.72968894103705,333.523993495455));
#21179=CARTESIAN_POINT('Ctrl Pts',(133.996122144138,-5.68832829519387,333.363436184663));
#21180=CARTESIAN_POINT('Ctrl Pts',(134.003927043548,-5.64025647230966,333.20478026353));
#21181=CARTESIAN_POINT('Ctrl Pts',(134.011731942957,-5.58568624137394,333.048580061743));
#21182=CARTESIAN_POINT('Ctrl Pts',(134.019555047678,-5.53098872268916,332.892015515299));
#21183=CARTESIAN_POINT('Ctrl Pts',(134.027378152399,-5.46976259593421,332.737918438187));
#21184=CARTESIAN_POINT('Ctrl Pts',(134.03520125712,-5.40226868233612,332.586822914424));
#21185=CARTESIAN_POINT('Ctrl Pts',(134.042096398524,-5.34278078146086,332.453650083554));
#21186=CARTESIAN_POINT('Ctrl Pts',(134.048991539929,-5.27842461240621,332.322808720411));
#21187=CARTESIAN_POINT('Ctrl Pts',(134.055886681333,-5.20940709427122,332.194646494886));
#21188=CARTESIAN_POINT('Ctrl Pts',(134.063310658771,-5.1350961458186,332.056654622794));
#21189=CARTESIAN_POINT('Ctrl Pts',(134.070734636209,-5.05518641366889,331.92140925387));
#21190=CARTESIAN_POINT('Ctrl Pts',(134.078158613647,-4.96990532954527,331.789397007125));
#21191=CARTESIAN_POINT('Ctrl Pts',(134.085573829675,-4.88472488993215,331.657540554694));
#21192=CARTESIAN_POINT('Ctrl Pts',(134.092989045702,-4.79418591677853,331.528909939925));
#21193=CARTESIAN_POINT('Ctrl Pts',(134.10040426173,-4.69856230686571,331.40396846357));
#21194=CARTESIAN_POINT('Ctrl Pts',(134.107812342874,-4.60303070550889,331.279147205274));
#21195=CARTESIAN_POINT('Ctrl Pts',(134.115220424018,-4.50242443258408,331.158008313049));
#21196=CARTESIAN_POINT('Ctrl Pts',(134.122628505162,-4.3970613072146,331.04098719084));
#21197=CARTESIAN_POINT('Ctrl Pts',(134.130031072336,-4.2917766055436,330.924053169589));
#21198=CARTESIAN_POINT('Ctrl Pts',(134.13743363951,-4.18174234995567,330.811231091794));
#21199=CARTESIAN_POINT('Ctrl Pts',(134.144836206684,-4.06731728257649,330.702924170397));
#21200=CARTESIAN_POINT('Ctrl Pts',(134.152234876439,-3.95295245949564,330.594674272122));
#21201=CARTESIAN_POINT('Ctrl Pts',(134.159633546194,-3.83420169896169,330.490935051799));
#21202=CARTESIAN_POINT('Ctrl Pts',(134.167032215949,-3.71146124206279,330.392073567084));
#21203=CARTESIAN_POINT('Ctrl Pts',(134.174429665153,-3.58874103352752,330.293228391444));
#21204=CARTESIAN_POINT('Ctrl Pts',(134.181827114357,-3.46203272526591,330.199259588275));
#21205=CARTESIAN_POINT('Ctrl Pts',(134.18922456356,-3.33176643274027,330.110494605774));
#21206=CARTESIAN_POINT('Ctrl Pts',(134.196621692024,-3.20150578833396,330.021733471968));
#21207=CARTESIAN_POINT('Ctrl Pts',(134.204018820487,-3.06768777481492,329.938175920366));
#21208=CARTESIAN_POINT('Ctrl Pts',(134.211415948951,-2.93077211676588,329.86010648339));
#21209=CARTESIAN_POINT('Ctrl Pts',(134.218814216388,-2.79383537712312,329.782025025669));
#21210=CARTESIAN_POINT('Ctrl Pts',(134.226212483824,-2.65380036748951,329.709433550022));
#21211=CARTESIAN_POINT('Ctrl Pts',(134.233610751261,-2.51115193253958,329.64257090255));
#21212=CARTESIAN_POINT('Ctrl Pts',(134.241011617787,-2.36845338369463,329.575684765527));
#21213=CARTESIAN_POINT('Ctrl Pts',(134.248412484312,-2.22313991926851,329.514531622055));
#21214=CARTESIAN_POINT('Ctrl Pts',(134.255813350838,-2.0757167518377,329.459302342787));
#21215=CARTESIAN_POINT('Ctrl Pts',(134.263222344223,-1.92813169967469,329.404012416491));
#21216=CARTESIAN_POINT('Ctrl Pts',(134.270631337608,-1.77843266772151,329.35465947618));
#21217=CARTESIAN_POINT('Ctrl Pts',(134.278040330992,-1.62714113460999,329.31138485301));
#21218=CARTESIAN_POINT('Ctrl Pts',(134.285453888573,-1.47575640069542,329.26808357118));
#21219=CARTESIAN_POINT('Ctrl Pts',(134.292867446153,-1.32277757256699,329.230868155821));
#21220=CARTESIAN_POINT('Ctrl Pts',(134.300281003733,-1.16873622563934,329.199828778615));
#21221=CARTESIAN_POINT('Ctrl Pts',(134.30770511587,-1.01447557265346,329.168745211173));
#21222=CARTESIAN_POINT('Ctrl Pts',(134.315129228006,-0.85914974723988,329.143855301598));
#21223=CARTESIAN_POINT('Ctrl Pts',(134.322553340143,-0.703296166356293,
329.125197444604));
#21224=CARTESIAN_POINT('Ctrl Pts',(134.326410465298,-0.622323956322832,
329.115503936718));
#21225=CARTESIAN_POINT('Ctrl Pts',(134.330267590452,-0.541209317292771,
329.107491738661));
#21226=CARTESIAN_POINT('Ctrl Pts',(134.334124715607,-0.460027482380483,
329.101160683833));
#21227=CARTESIAN_POINT('Ctrl Pts',(134.341548693045,-0.30377325504216,329.088975025781));
#21228=CARTESIAN_POINT('Ctrl Pts',(134.348972670483,-0.146798797695722,
329.082983794843));
#21229=CARTESIAN_POINT('Ctrl Pts',(134.356396647921,0.0103636049962139,
329.0832590763));
#21230=CARTESIAN_POINT('Ctrl Pts',(134.363811863948,0.167340532406615,329.083534032883));
#21231=CARTESIAN_POINT('Ctrl Pts',(134.371227079976,0.324504594077193,329.090060780498));
#21232=CARTESIAN_POINT('Ctrl Pts',(134.378642296003,0.481317969259022,329.102859712117));
#21233=CARTESIAN_POINT('Ctrl Pts',(134.386050377148,0.637980459400758,329.115646328669));
#21234=CARTESIAN_POINT('Ctrl Pts',(134.393458458292,0.794292565323229,329.134693084381));
#21235=CARTESIAN_POINT('Ctrl Pts',(134.400866539436,0.949716156397051,329.15996834043));
#21236=CARTESIAN_POINT('Ctrl Pts',(134.40826910661,1.10502406285349,329.185224783644));
#21237=CARTESIAN_POINT('Ctrl Pts',(134.415671673784,1.25944440448697,329.216700436622));
#21238=CARTESIAN_POINT('Ctrl Pts',(134.423074240958,1.41244397498346,329.254311827115));
#21239=CARTESIAN_POINT('Ctrl Pts',(134.430472910712,1.56536299187487,329.291903415375));
#21240=CARTESIAN_POINT('Ctrl Pts',(134.437871580467,1.71686236586658,329.335624218672));
#21241=CARTESIAN_POINT('Ctrl Pts',(134.445270250222,1.86641900155446,329.385339665382));
#21242=CARTESIAN_POINT('Ctrl Pts',(134.452667699426,2.01595096504142,329.435046910586));
#21243=CARTESIAN_POINT('Ctrl Pts',(134.46006514863,2.16354047248464,329.490746718882));
#21244=CARTESIAN_POINT('Ctrl Pts',(134.467462597834,2.30867940555075,329.552254598012));
#21245=CARTESIAN_POINT('Ctrl Pts',(134.474859726297,2.4538120456457,329.613759810267));
#21246=CARTESIAN_POINT('Ctrl Pts',(134.482256854761,2.59649397900092,329.681072447013));
#21247=CARTESIAN_POINT('Ctrl Pts',(134.489653983224,2.73623715288133,329.753959892863));
#21248=CARTESIAN_POINT('Ctrl Pts',(134.497052250661,2.87600184372211,329.82685856156));
#21249=CARTESIAN_POINT('Ctrl Pts',(134.504450518098,3.01282654318477,329.905333575905));
#21250=CARTESIAN_POINT('Ctrl Pts',(134.511848785534,3.14624802321231,329.989106473));
#21251=CARTESIAN_POINT('Ctrl Pts',(134.51924965206,3.27971637560892,330.072908800394));
#21252=CARTESIAN_POINT('Ctrl Pts',(134.526650518586,3.40977881228578,330.162012517857));
#21253=CARTESIAN_POINT('Ctrl Pts',(134.534051385111,3.53600142652282,330.256096072418));
#21254=CARTESIAN_POINT('Ctrl Pts',(134.541460378496,3.66236264525769,330.350282939716));
#21255=CARTESIAN_POINT('Ctrl Pts',(134.548869371881,3.78487532158267,330.449460341501));
#21256=CARTESIAN_POINT('Ctrl Pts',(134.556278365266,3.90313840510259,330.553266237662));
#21257=CARTESIAN_POINT('Ctrl Pts',(134.563691922846,4.02147434276138,330.657136081837));
#21258=CARTESIAN_POINT('Ctrl Pts',(134.571105480426,4.13555520131591,330.765639845399));
#21259=CARTESIAN_POINT('Ctrl Pts',(134.578519038006,4.24501748751773,330.878379312313));
#21260=CARTESIAN_POINT('Ctrl Pts',(134.585943150143,4.35463561332356,330.991279284498));
#21261=CARTESIAN_POINT('Ctrl Pts',(134.59336726228,4.45962178601344,331.108426726565));
#21262=CARTESIAN_POINT('Ctrl Pts',(134.600791374417,4.55965289150053,331.229390490712));
#21263=CARTESIAN_POINT('Ctrl Pts',(134.604648499571,4.61162307811934,331.292236036268));
#21264=CARTESIAN_POINT('Ctrl Pts',(134.608505624726,4.66225649193679,331.356111206627));
#21265=CARTESIAN_POINT('Ctrl Pts',(134.612362749881,4.71151256009419,331.420952646503));
#21266=CARTESIAN_POINT('Ctrl Pts',(134.619786727318,4.8063178681985,331.545755801024));
#21267=CARTESIAN_POINT('Ctrl Pts',(134.627210704756,4.89630390817413,331.674516772272));
#21268=CARTESIAN_POINT('Ctrl Pts',(134.634634682194,4.98112201219741,331.806826960201));
#21269=CARTESIAN_POINT('Ctrl Pts',(134.642049898222,5.0658400180964,331.9389810022));
#21270=CARTESIAN_POINT('Ctrl Pts',(134.64946511425,5.14540202862682,332.074675612246));
#21271=CARTESIAN_POINT('Ctrl Pts',(134.656880330277,5.21949984923519,332.213469561204));
#21272=CARTESIAN_POINT('Ctrl Pts',(134.664288411421,5.29352637329363,332.352129963324));
#21273=CARTESIAN_POINT('Ctrl Pts',(134.671696492565,5.36209899977196,332.493883440385));
#21274=CARTESIAN_POINT('Ctrl Pts',(134.679104573709,5.42495312107051,332.638260345278));
#21275=CARTESIAN_POINT('Ctrl Pts',(134.686507140883,5.48776045889865,332.782529787803));
#21276=CARTESIAN_POINT('Ctrl Pts',(134.693909708057,5.54485761830156,332.929418429395));
#21277=CARTESIAN_POINT('Ctrl Pts',(134.701312275231,5.59602624434115,333.078432713865));
#21278=CARTESIAN_POINT('Ctrl Pts',(134.708710944986,5.64716793032276,333.227368542965));
#21279=CARTESIAN_POINT('Ctrl Pts',(134.716109614741,5.69238717838704,333.378427434015));
#21280=CARTESIAN_POINT('Ctrl Pts',(134.723508284495,5.73151407574537,333.531096680502));
#21281=CARTESIAN_POINT('Ctrl Pts',(134.730905733699,5.7706345183806,333.683740741303));
#21282=CARTESIAN_POINT('Ctrl Pts',(134.738303182903,5.80366451244279,333.83799426912));
#21283=CARTESIAN_POINT('Ctrl Pts',(134.745700632107,5.83048422942221,333.993330137056));
#21284=CARTESIAN_POINT('Ctrl Pts',(134.753097760571,5.85730278354544,334.148659269901));
#21285=CARTESIAN_POINT('Ctrl Pts',(134.760494889034,5.8779115324792,334.305070281786));
#21286=CARTESIAN_POINT('Ctrl Pts',(134.767892017498,5.89224197412736,334.462026877222));
#21287=CARTESIAN_POINT('Ctrl Pts',(134.775290284934,5.90657462230582,334.619007640055));
#21288=CARTESIAN_POINT('Ctrl Pts',(134.782688552371,5.91462700443071,334.776533782018));
#21289=CARTESIAN_POINT('Ctrl Pts',(134.790086819807,5.91638260661324,334.934065072501));
#21290=CARTESIAN_POINT('Ctrl Pts',(134.797487686333,5.91813882555728,335.091651705383));
#21291=CARTESIAN_POINT('Ctrl Pts',(134.804888552859,5.91359385606546,335.249243117434));
#21292=CARTESIAN_POINT('Ctrl Pts',(134.812289419384,5.90278328706665,335.406300416474));
#21293=CARTESIAN_POINT('Ctrl Pts',(134.819698412769,5.89196084702955,335.563530179442));
#21294=CARTESIAN_POINT('Ctrl Pts',(134.827107406154,5.87485909294768,335.720224285561));
#21295=CARTESIAN_POINT('Ctrl Pts',(134.834516399539,5.8515654406907,335.875849562319));
#21296=CARTESIAN_POINT('Ctrl Pts',(134.841929957119,5.82825743874044,336.031570709616));
#21297=CARTESIAN_POINT('Ctrl Pts',(134.849343514699,5.79875000765694,336.186221349791));
#21298=CARTESIAN_POINT('Ctrl Pts',(134.856757072279,5.76318130874689,336.339280316069));
#21299=CARTESIAN_POINT('Ctrl Pts',(134.864181184416,5.72756197128225,336.492557189807));
#21300=CARTESIAN_POINT('Ctrl Pts',(134.871605296553,5.685864230165,336.644237505025));
#21301=CARTESIAN_POINT('Ctrl Pts',(134.879029408689,5.63827579120752,336.793816229379));
#21302=CARTESIAN_POINT('Ctrl Pts',(134.882886533844,5.61355168122619,336.871528398822));
#21303=CARTESIAN_POINT('Ctrl Pts',(134.886743658999,5.58723833331448,336.948673636558));
#21304=CARTESIAN_POINT('Ctrl Pts',(134.890600784154,5.55936706798296,337.025183538825));
#21305=CARTESIAN_POINT('Ctrl Pts',(134.898024761592,5.50572202493012,337.172445493107));
#21306=CARTESIAN_POINT('Ctrl Pts',(134.90544873903,5.44614078684118,337.317796623737));
#21307=CARTESIAN_POINT('Ctrl Pts',(134.912872716468,5.38077827004688,337.46072261157));
#21308=CARTESIAN_POINT('Ctrl Pts',(134.920287932495,5.31549289085666,337.603479925233));
#21309=CARTESIAN_POINT('Ctrl Pts',(134.927703148523,5.24443996751648,337.743817456921));
#21310=CARTESIAN_POINT('Ctrl Pts',(134.935118364551,5.16782375726106,337.881237264855));
#21311=CARTESIAN_POINT('Ctrl Pts',(134.942526445695,5.09128126673744,338.018524848142));
#21312=CARTESIAN_POINT('Ctrl Pts',(134.949934526839,5.0091863265827,338.152899972931));
#21313=CARTESIAN_POINT('Ctrl Pts',(134.957342607983,4.92179067871552,338.283885972047));
#21314=CARTESIAN_POINT('Ctrl Pts',(134.964745175157,4.8344600810252,338.414774475892));
#21315=CARTESIAN_POINT('Ctrl Pts',(134.972147742331,4.74183683776611,338.542278567782));
#21316=CARTESIAN_POINT('Ctrl Pts',(134.979550309505,4.64421782647985,338.665947536819));
#21317=CARTESIAN_POINT('Ctrl Pts',(134.98694897926,4.54665021117636,338.789551394683));
#21318=CARTESIAN_POINT('Ctrl Pts',(134.994347649015,4.44409229679957,338.909323858795));
#21319=CARTESIAN_POINT('Ctrl Pts',(135.00174631877,4.3368832796346,339.024844590953));
#21320=CARTESIAN_POINT('Ctrl Pts',(135.009143767974,4.22969194862836,339.140346265778));
#21321=CARTESIAN_POINT('Ctrl Pts',(135.016541217178,4.11785129128037,339.251597327416));
#21322=CARTESIAN_POINT('Ctrl Pts',(135.023938666382,4.00173973375924,339.358211750908));
#21323=CARTESIAN_POINT('Ctrl Pts',(135.031335794845,3.88563321063289,339.464821551785));
#21324=CARTESIAN_POINT('Ctrl Pts',(135.038732923309,3.7652564304331,339.566794861825));
#21325=CARTESIAN_POINT('Ctrl Pts',(135.046130051772,3.64102330506524,339.663783855891));
#21326=CARTESIAN_POINT('Ctrl Pts',(135.053528319209,3.51677105089727,339.760787783842));
#21327=CARTESIAN_POINT('Ctrl Pts',(135.060926586646,3.38866156346105,339.852805638024));
#21328=CARTESIAN_POINT('Ctrl Pts',(135.068324854082,3.257140197588,339.939531181778));
#21329=CARTESIAN_POINT('Ctrl Pts',(135.075725720608,3.12557262687596,340.026287193127));
#21330=CARTESIAN_POINT('Ctrl Pts',(135.083126587134,2.99059110263412,340.107746986973));
#21331=CARTESIAN_POINT('Ctrl Pts',(135.09052745366,2.85266805000558,340.183648865324));
#21332=CARTESIAN_POINT('Ctrl Pts',(135.097936447044,2.71459354467929,340.259634091195));
#21333=CARTESIAN_POINT('Ctrl Pts',(135.105345440429,2.5735713874897,340.330049033264));
#21334=CARTESIAN_POINT('Ctrl Pts',(135.112754433814,2.43009724031796,340.394678671163));
#21335=CARTESIAN_POINT('Ctrl Pts',(135.120167991394,2.28653470812265,340.459348123148));
#21336=CARTESIAN_POINT('Ctrl Pts',(135.127581548974,2.14051752137725,340.518225030087));
#21337=CARTESIAN_POINT('Ctrl Pts',(135.134995106555,1.9925587073517,340.571143541523));
#21338=CARTESIAN_POINT('Ctrl Pts',(135.142419218691,1.8443892468669,340.624137392149));
#21339=CARTESIAN_POINT('Ctrl Pts',(135.149843330828,1.69427299350774,340.67115579404));
#21340=CARTESIAN_POINT('Ctrl Pts',(135.157267442965,1.54273621813229,340.712083291039));
#21341=CARTESIAN_POINT('Ctrl Pts',(135.161124568119,1.46400676235506,340.733346773497));
#21342=CARTESIAN_POINT('Ctrl Pts',(135.164981693274,1.38489402371016,340.752967032599));
#21343=CARTESIAN_POINT('Ctrl Pts',(135.168838818429,1.30547247370716,340.770933389227));
#21344=CARTESIAN_POINT('Ctrl Pts',(135.176262795867,1.15260634370706,340.805514021408));
#21345=CARTESIAN_POINT('Ctrl Pts',(135.183686773305,0.998134650330004,340.834068724219));
#21346=CARTESIAN_POINT('Ctrl Pts',(135.191110750743,0.842573729630976,340.856449442507));
#21347=CARTESIAN_POINT('Ctrl Pts',(135.19852596677,0.687196394223663,340.878803748179));
#21348=CARTESIAN_POINT('Ctrl Pts',(135.205941182798,0.530732756022619,340.894998520057));
#21349=CARTESIAN_POINT('Ctrl Pts',(135.213356398825,0.373712080201323,340.904936057538));
#21350=CARTESIAN_POINT('Ctrl Pts',(135.22076447997,0.216842488883807,340.914864033171));
#21351=CARTESIAN_POINT('Ctrl Pts',(135.228172561114,0.0594172969566546,
340.918546737042));
#21352=CARTESIAN_POINT('Ctrl Pts',(135.235580642258,-0.0980264239861944,
340.915937912343));
#21353=CARTESIAN_POINT('Ctrl Pts',(135.242983209432,-0.255352956691995,
340.91333102944));
#21354=CARTESIAN_POINT('Ctrl Pts',(135.250385776606,-0.412697619390957,
340.904441948458));
#21355=CARTESIAN_POINT('Ctrl Pts',(135.25778834378,-0.569520742199788,340.889276414527));
#21356=CARTESIAN_POINT('Ctrl Pts',(135.265187013534,-0.726261298319962,
340.874118865183));
#21357=CARTESIAN_POINT('Ctrl Pts',(135.272585683289,-0.882480490866497,
340.85269147988));
#21358=CARTESIAN_POINT('Ctrl Pts',(135.279984353044,-1.03764128990488,340.825052026891));
#21359=CARTESIAN_POINT('Ctrl Pts',(135.287381802248,-1.19277649222948,340.797417133553));
#21360=CARTESIAN_POINT('Ctrl Pts',(135.294779251452,-1.34685328050463,340.76357227181));
#21361=CARTESIAN_POINT('Ctrl Pts',(135.302176700656,-1.49934224999276,340.723626768045));
#21362=CARTESIAN_POINT('Ctrl Pts',(135.309573829119,-1.65182460782507,340.683682996248));
#21363=CARTESIAN_POINT('Ctrl Pts',(135.316970957582,-1.80271892272736,340.637639202942));
#21364=CARTESIAN_POINT('Ctrl Pts',(135.324368086046,-1.95150870963899,340.585655227339));
#21365=CARTESIAN_POINT('Ctrl Pts',(135.331766353482,-2.1003214064634,340.533663247502));
#21366=CARTESIAN_POINT('Ctrl Pts',(135.339164620919,-2.24702857773313,340.475729387303));
#21367=CARTESIAN_POINT('Ctrl Pts',(135.346562888356,-2.3911316954519,340.412062432891));
#21368=CARTESIAN_POINT('Ctrl Pts',(135.353963754881,-2.5352854381114,340.348373111608));
#21369=CARTESIAN_POINT('Ctrl Pts',(135.361364621407,-2.6768329646302,340.27894683678));
#21370=CARTESIAN_POINT('Ctrl Pts',(135.368765487933,-2.8152985512318,340.204039260991));
#21371=CARTESIAN_POINT('Ctrl Pts',(135.376174481318,-2.95391618628547,340.129049429521));
#21372=CARTESIAN_POINT('Ctrl Pts',(135.383583474702,-3.08944479441327,340.048566454527));
#21373=CARTESIAN_POINT('Ctrl Pts',(135.390992468087,-3.22143532931494,339.962890788799));
#21374=CARTESIAN_POINT('Ctrl Pts',(135.398406025667,-3.3535071749389,339.877162343905));
#21375=CARTESIAN_POINT('Ctrl Pts',(135.405819583247,-3.48203630027982,339.786235049131));
#21376=CARTESIAN_POINT('Ctrl Pts',(135.413233140828,-3.60660560965785,339.690450568856));
#21377=CARTESIAN_POINT('Ctrl Pts',(135.420657252964,-3.73135226625324,339.594529721838));
#21378=CARTESIAN_POINT('Ctrl Pts',(135.428081365101,-3.85212756185855,339.493738116977));
#21379=CARTESIAN_POINT('Ctrl Pts',(135.435505477238,-3.96854961156869,339.388455826714));
#21380=CARTESIAN_POINT('Ctrl Pts',(135.439362602392,-4.02903555362147,339.333757438188));
#21381=CARTESIAN_POINT('Ctrl Pts',(135.443219727547,-4.08834709044893,339.277847496475));
#21382=CARTESIAN_POINT('Ctrl Pts',(135.447076852702,-4.14643494094762,339.220782847173));
#21383=CARTESIAN_POINT('Ctrl Pts',(135.45439526703,-4.25664939870424,339.112509786182));
#21384=CARTESIAN_POINT('Ctrl Pts',(135.461713681359,-4.36280933909392,338.999730679644));
#21385=CARTESIAN_POINT('Ctrl Pts',(135.469032095688,-4.4645159647071,338.882786082618));
#21386=CARTESIAN_POINT('Ctrl Pts',(135.476341726381,-4.56610052098445,338.765981843699));
#21387=CARTESIAN_POINT('Ctrl Pts',(135.483651357074,-4.66324214693022,338.645022348695));
#21388=CARTESIAN_POINT('Ctrl Pts',(135.490960987767,-4.75557691634672,338.520286743322));
#21389=CARTESIAN_POINT('Ctrl Pts',(135.498350180789,-4.84891671182039,338.394193442095));
#21390=CARTESIAN_POINT('Ctrl Pts',(135.505739373811,-4.93734408256862,338.26424159311));
#21391=CARTESIAN_POINT('Ctrl Pts',(135.513128566833,-5.02052234680356,338.130860253628));
#21392=CARTESIAN_POINT('Ctrl Pts',(135.520425267282,-5.10265944569908,337.999148485264));
#21393=CARTESIAN_POINT('Ctrl Pts',(135.527721967731,-5.17967786748907,337.864092916784));
#21394=CARTESIAN_POINT('Ctrl Pts',(135.53501866818,-5.25129509341039,337.72613836854));
#21395=CARTESIAN_POINT('Ctrl Pts',(135.542312273334,-5.32288193896001,337.588242341278));
#21396=CARTESIAN_POINT('Ctrl Pts',(135.549605878488,-5.38907197012852,337.447450121665));
#21397=CARTESIAN_POINT('Ctrl Pts',(135.556899483641,-5.44962772291846,337.304232680113));
#21398=CARTESIAN_POINT('Ctrl Pts',(135.564191530132,-5.51017053478007,337.161045844516));
#21399=CARTESIAN_POINT('Ctrl Pts',(135.571483576623,-5.56508131525385,337.015435172785));
#21400=CARTESIAN_POINT('Ctrl Pts',(135.578775623113,-5.61417014868265,336.867892958427));
#21401=CARTESIAN_POINT('Ctrl Pts',(135.586236122878,-5.66439298129037,336.716942377273));
#21402=CARTESIAN_POINT('Ctrl Pts',(135.593696622643,-5.70852144370212,336.563970311823));
#21403=CARTESIAN_POINT('Ctrl Pts',(135.601157122408,-5.74640579729457,336.409521541275));
#21404=CARTESIAN_POINT('Ctrl Pts',(135.608453037332,-5.78345439047947,336.258480039301));
#21405=CARTESIAN_POINT('Ctrl Pts',(135.615748952256,-5.8145314537954,336.106026699703));
#21406=CARTESIAN_POINT('Ctrl Pts',(135.62304486718,-5.83954861303036,335.952681771923));
#21407=CARTESIAN_POINT('Ctrl Pts',(135.630587659365,-5.86541229635978,335.794147998564));
#21408=CARTESIAN_POINT('Ctrl Pts',(135.638130451551,-5.88479868119094,335.634661679324));
#21409=CARTESIAN_POINT('Ctrl Pts',(135.645673243737,-5.89766840383677,335.474803075901));
#21410=CARTESIAN_POINT('Ctrl Pts',(135.653216035923,-5.9105381264826,335.314944472479));
#21411=CARTESIAN_POINT('Ctrl Pts',(135.660758828108,-5.91689121004861,335.154714037125));
#21412=CARTESIAN_POINT('Ctrl Pts',(135.668301620294,-5.91674761796713,334.994690783454));
#21413=CARTESIAN_POINT('',(137.418301620294,-5.92471687767985,335.002930573287));
#21414=CARTESIAN_POINT('Ctrl Pts',(135.668301620294,-5.91841553383544,334.9946892868));
#21415=CARTESIAN_POINT('Ctrl Pts',(135.687306042521,-5.92215085104165,334.591385784948));
#21416=CARTESIAN_POINT('Ctrl Pts',(135.799056476177,-5.70049280571943,332.223948443518));
#21417=CARTESIAN_POINT('Ctrl Pts',(136.003552921246,-2.51124033804167,328.469586928391));
#21418=CARTESIAN_POINT('Ctrl Pts',(136.281790955525,4.13258743031318,329.354263196709));
#21419=CARTESIAN_POINT('Ctrl Pts',(136.560028989797,6.98400071075933,335.419948798467));
#21420=CARTESIAN_POINT('Ctrl Pts',(136.838267024072,3.42629962262258,341.100253586306));
#21421=CARTESIAN_POINT('Ctrl Pts',(137.116505058345,-3.27566605709539,341.182445697587));
#21422=CARTESIAN_POINT('Ctrl Pts',(137.309849923753,-5.84393503100964,337.297073785147));
#21423=CARTESIAN_POINT('Ctrl Pts',(137.410448777736,-5.92572569476417,335.169119395345));
#21424=CARTESIAN_POINT('Ctrl Pts',(137.418301620294,-5.92471687767985,335.002930573287));
#21425=CARTESIAN_POINT('',(139.168300422869,-5.91261848715546,335.003766165052));
#21426=CARTESIAN_POINT('Ctrl Pts',(137.418301620294,-5.92471687767985,335.002930573287));
#21427=CARTESIAN_POINT('Ctrl Pts',(137.503194789161,-5.91381105874106,333.206346007866));
#21428=CARTESIAN_POINT('Ctrl Pts',(137.680833969451,-4.08295784035911,329.427749411782));
#21429=CARTESIAN_POINT('Ctrl Pts',(137.951219161168,2.35033272298692,328.409965173652));
#21430=CARTESIAN_POINT('Ctrl Pts',(138.229457195441,6.81360077617479,333.410198948256));
#21431=CARTESIAN_POINT('Ctrl Pts',(138.507695229716,5.02412796564901,339.869369682618));
#21432=CARTESIAN_POINT('Ctrl Pts',(138.78593326399,-1.37591292294527,341.859991731022));
#21433=CARTESIAN_POINT('Ctrl Pts',(139.006134687901,-5.44171109823543,338.453199721582));
#21434=CARTESIAN_POINT('Ctrl Pts',(139.133590100387,-5.91369737005363,335.74321261132));
#21435=CARTESIAN_POINT('Ctrl Pts',(139.16829950145,-5.9094401988413,335.003783783589));
#21436=CARTESIAN_POINT('',(140.918302830788,-5.91342774936137,334.995424942681));
#21437=CARTESIAN_POINT('Ctrl Pts',(139.168301620294,-5.9167488158986,335.00374326897));
#21438=CARTESIAN_POINT('Ctrl Pts',(139.175753102405,-5.91684936887011,334.844805538364));
#21439=CARTESIAN_POINT('Ctrl Pts',(139.183204584516,-5.91054143042238,334.685840579607));
#21440=CARTESIAN_POINT('Ctrl Pts',(139.190656066627,-5.89784510831784,334.527396952198));
#21441=CARTESIAN_POINT('Ctrl Pts',(139.19810809896,-5.88514784870938,334.368941625219));
#21442=CARTESIAN_POINT('Ctrl Pts',(139.205560131292,-5.86606129405076,334.211008070705));
#21443=CARTESIAN_POINT('Ctrl Pts',(139.213012163625,-5.84065751797578,334.054140433144));
#21444=CARTESIAN_POINT('Ctrl Pts',(139.220466135568,-5.8152471298227,333.897231966177));
#21445=CARTESIAN_POINT('Ctrl Pts',(139.227920107511,-5.78351630303407,333.741390329624));
#21446=CARTESIAN_POINT('Ctrl Pts',(139.235374079454,-5.74558837734309,333.58715012806));
#21447=CARTESIAN_POINT('Ctrl Pts',(139.242831381279,-5.70764350826209,333.432841023391));
#21448=CARTESIAN_POINT('Ctrl Pts',(139.250288683105,-5.66349611268614,333.280135133418));
#21449=CARTESIAN_POINT('Ctrl Pts',(139.257745984931,-5.61331957911448,333.129552495997));
#21450=CARTESIAN_POINT('Ctrl Pts',(139.265212769917,-5.56307923800034,332.978778368504));
#21451=CARTESIAN_POINT('Ctrl Pts',(139.272679554903,-5.50679455822665,332.83013323447));
#21452=CARTESIAN_POINT('Ctrl Pts',(139.280146339889,-5.44468769455522,332.684118640504));
#21453=CARTESIAN_POINT('Ctrl Pts',(139.28761818195,-5.38253876738727,332.538005154339));
#21454=CARTESIAN_POINT('Ctrl Pts',(139.295090024011,-5.31455995236136,332.394526089145));
#21455=CARTESIAN_POINT('Ctrl Pts',(139.302561866072,-5.24101952035768,332.254158608053));
#21456=CARTESIAN_POINT('Ctrl Pts',(139.310045923778,-5.16735885779002,332.113561641479));
#21457=CARTESIAN_POINT('Ctrl Pts',(139.317529981484,-5.08811859171075,331.976086740265));
#21458=CARTESIAN_POINT('Ctrl Pts',(139.32501403919,-5.00361112229794,331.842183301818));
#21459=CARTESIAN_POINT('Ctrl Pts',(139.330812470306,-4.93813718297193,331.738438796565));
#21460=CARTESIAN_POINT('Ctrl Pts',(139.336610901421,-4.86950239493759,331.636837564401));
#21461=CARTESIAN_POINT('Ctrl Pts',(139.342409332537,-4.79786834624722,331.537574564763));
#21462=CARTESIAN_POINT('Ctrl Pts',(139.349833309975,-4.70615223361802,331.410483933685));
#21463=CARTESIAN_POINT('Ctrl Pts',(139.357257287413,-4.60924452397342,331.286848295946));
#21464=CARTESIAN_POINT('Ctrl Pts',(139.364681264851,-4.50743432440201,331.167120354916));
#21465=CARTESIAN_POINT('Ctrl Pts',(139.372096480879,-4.40574427618426,331.04753371087));
#21466=CARTESIAN_POINT('Ctrl Pts',(139.379511696906,-4.29916349393508,330.931845865481));
#21467=CARTESIAN_POINT('Ctrl Pts',(139.386926912934,-4.18802410190193,330.820480328508));
#21468=CARTESIAN_POINT('Ctrl Pts',(139.394334994078,-4.07699164763216,330.709221946894));
#21469=CARTESIAN_POINT('Ctrl Pts',(139.401743075222,-3.96140957769699,330.602277856496));
#21470=CARTESIAN_POINT('Ctrl Pts',(139.409151156366,-3.84164991394839,330.5000381667));
#21471=CARTESIAN_POINT('Ctrl Pts',(139.41655372354,-3.72197938950464,330.397874575771));
#21472=CARTESIAN_POINT('Ctrl Pts',(139.423956290715,-3.59813774526255,330.300408654587));
#21473=CARTESIAN_POINT('Ctrl Pts',(139.431358857889,-3.470533365601,330.207993247005));
#21474=CARTESIAN_POINT('Ctrl Pts',(139.438757527643,-3.34299616908793,330.115626495732));
#21475=CARTESIAN_POINT('Ctrl Pts',(139.446156197398,-3.21170048406593,330.028305180718));
#21476=CARTESIAN_POINT('Ctrl Pts',(139.453554867153,-3.07708714444699,329.946341397762));
#21477=CARTESIAN_POINT('Ctrl Pts',(139.460952316357,-2.94249601184888,329.864391136283));
#21478=CARTESIAN_POINT('Ctrl Pts',(139.468349765561,-2.80458862934737,329.787796846657));
#21479=CARTESIAN_POINT('Ctrl Pts',(139.475747214765,-2.66383423526644,329.71682692603));
#21480=CARTESIAN_POINT('Ctrl Pts',(139.483144343228,-2.5230859440508,329.645860082535));
#21481=CARTESIAN_POINT('Ctrl Pts',(139.490541471692,-2.37949121994516,329.580517291188));
#21482=CARTESIAN_POINT('Ctrl Pts',(139.497938600155,-2.23354304473216,329.52102053026));
#21483=CARTESIAN_POINT('Ctrl Pts',(139.505336867592,-2.08757239714333,329.461514608317));
#21484=CARTESIAN_POINT('Ctrl Pts',(139.512735135029,-1.93924792253438,329.407856649989));
#21485=CARTESIAN_POINT('Ctrl Pts',(139.520133402465,-1.78908153339491,329.360220054881));
#21486=CARTESIAN_POINT('Ctrl Pts',(139.527534268991,-1.63886238922354,329.312566724536));
#21487=CARTESIAN_POINT('Ctrl Pts',(139.534935135517,-1.48680039769533,329.270939081883));
#21488=CARTESIAN_POINT('Ctrl Pts',(139.542336002043,-1.33342139130082,329.235460299753));
#21489=CARTESIAN_POINT('Ctrl Pts',(139.549744995427,-1.17987396009384,329.199942558529));
#21490=CARTESIAN_POINT('Ctrl Pts',(139.557153988812,-1.02500698969268,329.170587246164));
#21491=CARTESIAN_POINT('Ctrl Pts',(139.564562982197,-0.869355961450153,
329.147466294434));
#21492=CARTESIAN_POINT('Ctrl Pts',(139.571976539777,-0.713609046805256,
329.124331099399));
#21493=CARTESIAN_POINT('Ctrl Pts',(139.579390097358,-0.557077482054096,
329.107437957816));
#21494=CARTESIAN_POINT('Ctrl Pts',(139.586803654938,-0.400300069283826,
329.096806760995));
#21495=CARTESIAN_POINT('Ctrl Pts',(139.594227767075,-0.243299455164703,
329.08616042872));
#21496=CARTESIAN_POINT('Ctrl Pts',(139.601651879211,-0.0860526660484347,
329.081793856626));
#21497=CARTESIAN_POINT('Ctrl Pts',(139.609075991348,0.0709024746906525,
329.083674839769));
#21498=CARTESIAN_POINT('Ctrl Pts',(139.612933116502,0.152446989411648,329.084652086241));
#21499=CARTESIAN_POINT('Ctrl Pts',(139.616790241656,0.233912870431467,329.087314831304));
#21500=CARTESIAN_POINT('Ctrl Pts',(139.620647366811,0.315225552318783,329.091653072672));
#21501=CARTESIAN_POINT('Ctrl Pts',(139.628071344249,0.471731626564145,329.100003075524));
#21502=CARTESIAN_POINT('Ctrl Pts',(139.635495321687,0.628141794240556,329.114588498208));
#21503=CARTESIAN_POINT('Ctrl Pts',(139.642919299125,0.783918914991726,329.135411208173));
#21504=CARTESIAN_POINT('Ctrl Pts',(139.650334515152,0.939512195302699,329.156209344208));
#21505=CARTESIAN_POINT('Ctrl Pts',(139.65774973118,1.09447354946046,329.183230066496));
#21506=CARTESIAN_POINT('Ctrl Pts',(139.665164947208,1.24826710758629,329.216423270102));
#21507=CARTESIAN_POINT('Ctrl Pts',(139.672573028352,1.40191268632479,329.249584535375));
#21508=CARTESIAN_POINT('Ctrl Pts',(139.679981109496,1.55439234363106,329.288906380054));
#21509=CARTESIAN_POINT('Ctrl Pts',(139.68738919064,1.70517670583118,329.334287073599));
#21510=CARTESIAN_POINT('Ctrl Pts',(139.694791757814,1.85584883647644,329.379633989465));
#21511=CARTESIAN_POINT('Ctrl Pts',(139.702194324988,2.00482782867516,329.431030667607));
#21512=CARTESIAN_POINT('Ctrl Pts',(139.709596892162,2.15159596827859,329.488324632946));
#21513=CARTESIAN_POINT('Ctrl Pts',(139.716995561917,2.2982868350989,329.545588433264));
#21514=CARTESIAN_POINT('Ctrl Pts',(139.724394231672,2.44276882072263,329.60874320182));
#21515=CARTESIAN_POINT('Ctrl Pts',(139.731792901426,2.58454091661175,329.677587124916));
#21516=CARTESIAN_POINT('Ctrl Pts',(139.73919035063,2.7262896245066,329.746419690902));
#21517=CARTESIAN_POINT('Ctrl Pts',(139.746587799834,2.86532899451625,329.820939385876));
#21518=CARTESIAN_POINT('Ctrl Pts',(139.753985249038,3.00117939397023,329.900896862417));
#21519=CARTESIAN_POINT('Ctrl Pts',(139.761382377502,3.13702390318764,329.980850872141));
#21520=CARTESIAN_POINT('Ctrl Pts',(139.768779505965,3.26967939513561,330.066242005334));
#21521=CARTESIAN_POINT('Ctrl Pts',(139.776176634429,3.39869242281925,330.156775828276));
#21522=CARTESIAN_POINT('Ctrl Pts',(139.783574901865,3.5277253152887,330.247323591167));
#21523=CARTESIAN_POINT('Ctrl Pts',(139.790973169302,3.65311432125548,330.343015406085));
#21524=CARTESIAN_POINT('Ctrl Pts',(139.798371436739,3.77443660007292,330.443514631371));
#21525=CARTESIAN_POINT('Ctrl Pts',(139.805772303264,3.89580150068341,330.544049163092));
#21526=CARTESIAN_POINT('Ctrl Pts',(139.81317316979,4.01309654240838,330.649394229835));
#21527=CARTESIAN_POINT('Ctrl Pts',(139.820574036316,4.1259335884536,330.759174303727));
#21528=CARTESIAN_POINT('Ctrl Pts',(139.827983029701,4.23889454036246,330.869074926635));
#21529=CARTESIAN_POINT('Ctrl Pts',(139.835392023086,4.34738745274674,330.983420022058));
#21530=CARTESIAN_POINT('Ctrl Pts',(139.84280101647,4.45106205695689,331.101798218714));
#21531=CARTESIAN_POINT('Ctrl Pts',(139.850214574051,4.55480052829927,331.220249340423));
#21532=CARTESIAN_POINT('Ctrl Pts',(139.857628131631,4.65371454292192,331.342738224437));
#21533=CARTESIAN_POINT('Ctrl Pts',(139.865041689211,4.74749579707092,331.468822544916));
#21534=CARTESIAN_POINT('Ctrl Pts',(139.872465801348,4.84141056600413,331.595086369508));
#21535=CARTESIAN_POINT('Ctrl Pts',(139.879889913485,4.93017777004392,331.724955546475));
#21536=CARTESIAN_POINT('Ctrl Pts',(139.887314025621,5.01353344392814,331.857960380722));
#21537=CARTESIAN_POINT('Ctrl Pts',(139.891171150776,5.05684007246314,331.927061746972));
#21538=CARTESIAN_POINT('Ctrl Pts',(139.89502827593,5.09868677606702,331.997009108466));
#21539=CARTESIAN_POINT('Ctrl Pts',(139.898885401085,5.13904161424091,332.067734348733));
#21540=CARTESIAN_POINT('Ctrl Pts',(139.906309378523,5.21671433579345,332.203862311142));
#21541=CARTESIAN_POINT('Ctrl Pts',(139.913733355961,5.28909165923555,332.343283967131));
#21542=CARTESIAN_POINT('Ctrl Pts',(139.921157333399,5.35588133671999,332.485548634498));
#21543=CARTESIAN_POINT('Ctrl Pts',(139.928572549426,5.42259219233598,332.627645408153));
#21544=CARTESIAN_POINT('Ctrl Pts',(139.935987765454,5.48372837091779,332.772578180098));
#21545=CARTESIAN_POINT('Ctrl Pts',(139.943402981481,5.53904201683372,332.919869211263));
#21546=CARTESIAN_POINT('Ctrl Pts',(139.950811062626,5.59430244023815,333.067018519741));
#21547=CARTESIAN_POINT('Ctrl Pts',(139.95821914377,5.64375135400219,333.216521223023));
#21548=CARTESIAN_POINT('Ctrl Pts',(139.965627224914,5.68718783103696,333.36787710726));
#21549=CARTESIAN_POINT('Ctrl Pts',(139.973029792088,5.73059197750871,333.51912033455));
#21550=CARTESIAN_POINT('Ctrl Pts',(139.980432359262,5.76799249545076,333.672213639101));
#21551=CARTESIAN_POINT('Ctrl Pts',(139.987834926436,5.79923743957738,333.826639151026));
#21552=CARTESIAN_POINT('Ctrl Pts',(139.99523359619,5.83046593337704,333.980983358593));
#21553=CARTESIAN_POINT('Ctrl Pts',(140.002632265945,5.85554523394587,334.136658011775));
#21554=CARTESIAN_POINT('Ctrl Pts',(140.0100309357,5.8743739262603,334.293132588831));
#21555=CARTESIAN_POINT('Ctrl Pts',(140.017428384904,5.89319951242533,334.449581352442));
#21556=CARTESIAN_POINT('Ctrl Pts',(140.024825834108,5.90577649230412,334.606829407846));
#21557=CARTESIAN_POINT('Ctrl Pts',(140.032223283312,5.91205499070205,334.764338485503));
#21558=CARTESIAN_POINT('Ctrl Pts',(140.039620411775,5.91833321687523,334.921840733841));
#21559=CARTESIAN_POINT('Ctrl Pts',(140.047017540238,5.91831348969795,335.079603609012));
#21560=CARTESIAN_POINT('Ctrl Pts',(140.054414668702,5.91199801857741,335.237086462787));
#21561=CARTESIAN_POINT('Ctrl Pts',(140.061812936138,5.90568157503197,335.39459356499));
#21562=CARTESIAN_POINT('Ctrl Pts',(140.069211203575,5.89306747232098,335.551820187011));
#21563=CARTESIAN_POINT('Ctrl Pts',(140.076609471012,5.87420997626101,335.708228577011));
#21564=CARTESIAN_POINT('Ctrl Pts',(140.084010337537,5.85534585536425,335.864691914925));
#21565=CARTESIAN_POINT('Ctrl Pts',(140.091411204063,5.83023401876787,336.020336078204));
#21566=CARTESIAN_POINT('Ctrl Pts',(140.098812070589,5.79898021278113,336.174631454658));
#21567=CARTESIAN_POINT('Ctrl Pts',(140.106221063974,5.76769208712762,336.329096262186));
#21568=CARTESIAN_POINT('Ctrl Pts',(140.113630057358,5.73024859715437,336.482208959058));
#21569=CARTESIAN_POINT('Ctrl Pts',(140.121039050743,5.68680612328484,336.633452380288));
#21570=CARTESIAN_POINT('Ctrl Pts',(140.128452608323,5.64333688735305,336.784788972683));
#21571=CARTESIAN_POINT('Ctrl Pts',(140.135866165903,5.59386142059843,336.934253641367));
#21572=CARTESIAN_POINT('Ctrl Pts',(140.143279723484,5.53858484340473,337.081347759243));
#21573=CARTESIAN_POINT('Ctrl Pts',(140.15070383562,5.4832295698835,337.228651292526));
#21574=CARTESIAN_POINT('Ctrl Pts',(140.158127947757,5.42205683590311,337.373577191717));
#21575=CARTESIAN_POINT('Ctrl Pts',(140.165552059894,5.35531877133848,337.515649303828));
#21576=CARTESIAN_POINT('Ctrl Pts',(140.169409185049,5.32064565987542,337.589461485993));
#21577=CARTESIAN_POINT('Ctrl Pts',(140.173266310204,5.2844710838117,337.662503802708));
#21578=CARTESIAN_POINT('Ctrl Pts',(140.177123435359,5.24683503890533,337.734712532793));
#21579=CARTESIAN_POINT('Ctrl Pts',(140.184547412797,5.17439529764409,337.873695832903));
#21580=CARTESIAN_POINT('Ctrl Pts',(140.191971390235,5.09632017541685,338.010008526357));
#21581=CARTESIAN_POINT('Ctrl Pts',(140.199395367673,5.01283050842129,338.143160965706));
#21582=CARTESIAN_POINT('Ctrl Pts',(140.2068105837,4.9294393717946,338.276156265144));
#21583=CARTESIAN_POINT('Ctrl Pts',(140.214225799728,4.84064660608486,338.405998421137));
#21584=CARTESIAN_POINT('Ctrl Pts',(140.221641015756,4.7467198233623,338.532220474574));
#21585=CARTESIAN_POINT('Ctrl Pts',(140.2290490969,4.65288341651675,338.658321077787));
#21586=CARTESIAN_POINT('Ctrl Pts',(140.236457178044,4.55392304844181,338.780808215528));
#21587=CARTESIAN_POINT('Ctrl Pts',(140.243865259188,4.45015062645744,338.899242229503));
#21588=CARTESIAN_POINT('Ctrl Pts',(140.251267826362,4.34645544418261,339.017588090878));
#21589=CARTESIAN_POINT('Ctrl Pts',(140.258670393536,4.23795558458325,339.131886555905));
#21590=CARTESIAN_POINT('Ctrl Pts',(140.26607296071,4.12500430918265,339.241729601439));
#21591=CARTESIAN_POINT('Ctrl Pts',(140.273471630465,4.01211250213469,339.35151481509));
#21592=CARTESIAN_POINT('Ctrl Pts',(140.280870300219,3.89477421368746,339.456849021429));
#21593=CARTESIAN_POINT('Ctrl Pts',(140.288268969974,3.77338068940207,339.557359842644));
#21594=CARTESIAN_POINT('Ctrl Pts',(140.295666419178,3.65200719127845,339.657854082695));
#21595=CARTESIAN_POINT('Ctrl Pts',(140.303063868382,3.5265800722271,339.753526279065));
#21596=CARTESIAN_POINT('Ctrl Pts',(140.310461317586,3.39752498425916,339.844043202102));
#21597=CARTESIAN_POINT('Ctrl Pts',(140.31785844605,3.26847549189494,339.934556200484));
#21598=CARTESIAN_POINT('Ctrl Pts',(140.325255574513,3.13579864893123,340.019914155667));
#21599=CARTESIAN_POINT('Ctrl Pts',(140.332652702977,2.99995029363697,340.099826349809));
#21600=CARTESIAN_POINT('Ctrl Pts',(140.340050970413,2.86408102108679,340.179750848434));
#21601=CARTESIAN_POINT('Ctrl Pts',(140.34744923785,2.72503958557102,340.254227727192));
#21602=CARTESIAN_POINT('Ctrl Pts',(140.354847505287,2.58330756043057,340.323011610989));
#21603=CARTESIAN_POINT('Ctrl Pts',(140.362248371812,2.44152574334001,340.391819659287));
#21604=CARTESIAN_POINT('Ctrl Pts',(140.369649238338,2.29705179021712,340.454930567766));
#21605=CARTESIAN_POINT('Ctrl Pts',(140.377050104864,2.15038828864746,340.512146657206));
#21606=CARTESIAN_POINT('Ctrl Pts',(140.384459098249,2.00356373653097,340.569425575383));
#21607=CARTESIAN_POINT('Ctrl Pts',(140.391868091633,1.8545451822827,340.620796611725));
#21608=CARTESIAN_POINT('Ctrl Pts',(140.399277085018,1.7038521473927,340.666111402216));
#21609=CARTESIAN_POINT('Ctrl Pts',(140.406690642598,1.55306628039536,340.711454108182));
#21610=CARTESIAN_POINT('Ctrl Pts',(140.414104200179,1.4006042378463,340.750733041181));
#21611=CARTESIAN_POINT('Ctrl Pts',(140.421517757759,1.24699632831833,340.783850855586));
#21612=CARTESIAN_POINT('Ctrl Pts',(140.428941869896,1.09316972980945,340.817015819263));
#21613=CARTESIAN_POINT('Ctrl Pts',(140.436365982032,0.938194372873399,340.844002082093));
#21614=CARTESIAN_POINT('Ctrl Pts',(140.443790094169,0.782607106657409,340.864763991766));
#21615=CARTESIAN_POINT('Ctrl Pts',(140.447647219324,0.701773257814375,340.875550639728));
#21616=CARTESIAN_POINT('Ctrl Pts',(140.451504344478,0.620774276604041,340.884658055706));
#21617=CARTESIAN_POINT('Ctrl Pts',(140.455361469633,0.539685391524491,340.892085389798));
#21618=CARTESIAN_POINT('Ctrl Pts',(140.462785447071,0.383610068795989,340.906381104487));
#21619=CARTESIAN_POINT('Ctrl Pts',(140.470209424509,0.226730888180403,340.914492688595));
#21620=CARTESIAN_POINT('Ctrl Pts',(140.477633401947,0.0695791118012303,
340.916340871662));
#21621=CARTESIAN_POINT('Ctrl Pts',(140.485048617974,-0.0873872018372228,
340.918186873595));
#21622=CARTESIAN_POINT('Ctrl Pts',(140.492463834002,-0.244625101325928,
340.913784183549));
#21623=CARTESIAN_POINT('Ctrl Pts',(140.49987905003,-0.401597090539684,340.903105143852));
#21624=CARTESIAN_POINT('Ctrl Pts',(140.507287131174,-0.558418042095502,
340.892436379474));
#21625=CARTESIAN_POINT('Ctrl Pts',(140.514695212318,-0.714973222878964,
340.875503313274));
#21626=CARTESIAN_POINT('Ctrl Pts',(140.522103293462,-0.870724123905083,
340.852330310445));
#21627=CARTESIAN_POINT('Ctrl Pts',(140.529505860636,-1.02635909669033,340.829174555704));
#21628=CARTESIAN_POINT('Ctrl Pts',(140.53690842781,-1.18119061413119,340.799788166895));
#21629=CARTESIAN_POINT('Ctrl Pts',(140.544310994984,-1.33468439078115,340.764247404432));
#21630=CARTESIAN_POINT('Ctrl Pts',(140.551709664739,-1.48809735362897,340.728725354026));
#21631=CARTESIAN_POINT('Ctrl Pts',(140.559108334493,-1.64017361569421,340.687055467094));
#21632=CARTESIAN_POINT('Ctrl Pts',(140.566507004248,-1.79038831110776,340.639365235374));
#21633=CARTESIAN_POINT('Ctrl Pts',(140.573904453452,-1.9405782257613,340.591682871062));
#21634=CARTESIAN_POINT('Ctrl Pts',(140.581301902656,-2.08890682789001,340.537982245907));
#21635=CARTESIAN_POINT('Ctrl Pts',(140.58869935186,-2.23486355284494,340.478440970081));
#21636=CARTESIAN_POINT('Ctrl Pts',(140.596096480323,-2.38081394937115,340.418902275861));
#21637=CARTESIAN_POINT('Ctrl Pts',(140.603493608787,-2.52439232764025,340.353523575465));
#21638=CARTESIAN_POINT('Ctrl Pts',(140.61089073725,-2.66510753657285,340.282530868911));
#21639=CARTESIAN_POINT('Ctrl Pts',(140.618289004687,-2.80584441213424,340.211527231254));
#21640=CARTESIAN_POINT('Ctrl Pts',(140.625687272124,-2.94371690732875,340.134908034389));
#21641=CARTESIAN_POINT('Ctrl Pts',(140.63308553956,-3.07825807403807,340.05294545707));
#21642=CARTESIAN_POINT('Ctrl Pts',(140.640486406086,-3.21284650647498,339.970954085435));
#21643=CARTESIAN_POINT('Ctrl Pts',(140.647887272612,-3.34410096177593,339.883615789918));
#21644=CARTESIAN_POINT('Ctrl Pts',(140.655288139137,-3.47158322828818,339.791246231574));
#21645=CARTESIAN_POINT('Ctrl Pts',(140.662697132522,-3.59920548251621,339.698775242624));
#21646=CARTESIAN_POINT('Ctrl Pts',(140.670106125907,-3.72304697331511,339.60126217662));
#21647=CARTESIAN_POINT('Ctrl Pts',(140.677515119292,-3.84270179533154,339.499063621984));
#21648=CARTESIAN_POINT('Ctrl Pts',(140.684928676872,-3.96243032884669,339.396802109512));
#21649=CARTESIAN_POINT('Ctrl Pts',(140.692342234452,-4.07796678107884,339.289849609767));
#21650=CARTESIAN_POINT('Ctrl Pts',(140.699755792033,-4.188942311616,339.178599391238));
#21651=CARTESIAN_POINT('Ctrl Pts',(140.707179904169,-4.30007583613704,339.067190787656));
#21652=CARTESIAN_POINT('Ctrl Pts',(140.714604016306,-4.40663521840024,338.951472519044));
#21653=CARTESIAN_POINT('Ctrl Pts',(140.722028128443,-4.5082915485246,338.831871328216));
#21654=CARTESIAN_POINT('Ctrl Pts',(140.725885253597,-4.56110610477527,338.769733694358));
#21655=CARTESIAN_POINT('Ctrl Pts',(140.729742378752,-4.61259792162402,338.706548468387));
#21656=CARTESIAN_POINT('Ctrl Pts',(140.733599503907,-4.662725573915,338.642378451625));
#21657=CARTESIAN_POINT('Ctrl Pts',(140.741295425423,-4.76274267534399,338.514343349601));
#21658=CARTESIAN_POINT('Ctrl Pts',(140.748991346939,-4.85764424144846,338.381978211866));
#21659=CARTESIAN_POINT('Ctrl Pts',(140.756687268455,-4.94703476755112,338.245732208784));
#21660=CARTESIAN_POINT('Ctrl Pts',(140.764101460594,-5.0331529191608,338.114473847735));
#21661=CARTESIAN_POINT('Ctrl Pts',(140.771515652732,-5.11415610924468,337.979614061909));
#21662=CARTESIAN_POINT('Ctrl Pts',(140.778929844871,-5.18973002977055,337.84158983328));
#21663=CARTESIAN_POINT('Ctrl Pts',(140.786336986061,-5.26523207896498,337.703696866665));
#21664=CARTESIAN_POINT('Ctrl Pts',(140.793744127251,-5.33531495722257,337.562645771215));
#21665=CARTESIAN_POINT('Ctrl Pts',(140.80115126844,-5.39970745023283,337.418902646739));
#21666=CARTESIAN_POINT('Ctrl Pts',(140.80855282343,-5.46405138073848,337.275267928162));
#21667=CARTESIAN_POINT('Ctrl Pts',(140.81595437842,-5.52271331729638,337.128945560625));
#21668=CARTESIAN_POINT('Ctrl Pts',(140.82335593341,-5.57546790057303,336.98042628042));
#21669=CARTESIAN_POINT('Ctrl Pts',(140.830753363167,-5.62819308124973,336.831989776966));
#21670=CARTESIAN_POINT('Ctrl Pts',(140.838150792923,-5.67501734023533,336.681359149259));
#21671=CARTESIAN_POINT('Ctrl Pts',(140.84554822268,-5.71576345500202,336.529045025159));
#21672=CARTESIAN_POINT('Ctrl Pts',(140.852943502287,-5.75649772643343,336.376775172942));
#21673=CARTESIAN_POINT('Ctrl Pts',(140.860338781894,-5.79115727330841,336.222823157763));
#21674=CARTESIAN_POINT('Ctrl Pts',(140.867734061501,-5.81961476231465,336.067714653243));
#21675=CARTESIAN_POINT('Ctrl Pts',(140.875128144217,-5.84806764560735,335.912631252319));
#21676=CARTESIAN_POINT('Ctrl Pts',(140.882522226932,-5.87032040608578,335.756392101837));
#21677=CARTESIAN_POINT('Ctrl Pts',(140.889916309647,-5.88629689205176,335.599532702296));
#21678=CARTESIAN_POINT('Ctrl Pts',(140.897311781641,-5.90227637985019,335.442643830339));
#21679=CARTESIAN_POINT('Ctrl Pts',(140.904707253635,-5.91197720194651,335.285134847513));
#21680=CARTESIAN_POINT('Ctrl Pts',(140.91210272563,-5.91537509813926,335.1275461125));
#21681=CARTESIAN_POINT('Ctrl Pts',(140.914169023851,-5.916324471873,335.083515748632));
#21682=CARTESIAN_POINT('Ctrl Pts',(140.916235322073,-5.91678212280831,335.039479167637));
#21683=CARTESIAN_POINT('Ctrl Pts',(140.918301620294,-5.91674824910051,334.995448157951));
#21684=CARTESIAN_POINT('',(142.668300681201,-5.92181077008912,334.998336726183));
#21685=CARTESIAN_POINT('Ctrl Pts',(140.91830369428,-5.9110591082604,334.99540838233));
#21686=CARTESIAN_POINT('Ctrl Pts',(140.949481642247,-5.91579322684826,334.331668430357));
#21687=CARTESIAN_POINT('Ctrl Pts',(141.073405601637,-5.50601630485396,331.699164255947));
#21688=CARTESIAN_POINT('Ctrl Pts',(141.290075572456,-1.63579549677484,328.197294948772));
#21689=CARTESIAN_POINT('Ctrl Pts',(141.568313606728,4.83531700169147,329.943090626247));
#21690=CARTESIAN_POINT('Ctrl Pts',(141.846551641003,6.86913045686709,336.329537396148));
#21691=CARTESIAN_POINT('Ctrl Pts',(142.124789675277,2.59924427997537,341.495887321548));
#21692=CARTESIAN_POINT('Ctrl Pts',(142.398705767854,-3.9525535038928,340.713403626196));
#21693=CARTESIAN_POINT('Ctrl Pts',(142.579875849006,-5.91886630634388,336.86865198698));
#21694=CARTESIAN_POINT('Ctrl Pts',(142.668299918733,-5.92591990352904,334.998351685574));
#21695=CARTESIAN_POINT('',(144.418301620294,-5.91612998447623,335.005450957973));
#21696=CARTESIAN_POINT('Ctrl Pts',(142.668301620294,-5.91674976100815,334.998318301469));
#21697=CARTESIAN_POINT('Ctrl Pts',(142.672622994804,-5.9167238219269,334.907056371931));
#21698=CARTESIAN_POINT('Ctrl Pts',(142.676944369314,-5.91458651643603,334.81582708582));
#21699=CARTESIAN_POINT('Ctrl Pts',(142.681265743824,-5.91034167140472,334.7246967313));
#21700=CARTESIAN_POINT('Ctrl Pts',(142.688689721262,-5.90304916906167,334.568137818322));
#21701=CARTESIAN_POINT('Ctrl Pts',(142.6961136987,-5.88952074126305,334.411632685024));
#21702=CARTESIAN_POINT('Ctrl Pts',(142.703537676138,-5.86975089183501,334.255718446889));
#21703=CARTESIAN_POINT('Ctrl Pts',(142.710952892166,-5.85000437380384,334.099988211013));
#21704=CARTESIAN_POINT('Ctrl Pts',(142.718368108193,-5.82403114240898,333.944847848869));
#21705=CARTESIAN_POINT('Ctrl Pts',(142.725783324221,-5.79187768125842,333.790833556602));
#21706=CARTESIAN_POINT('Ctrl Pts',(142.733191405365,-5.75975515800627,333.636967456111));
#21707=CARTESIAN_POINT('Ctrl Pts',(142.740599486509,-5.72146431930344,333.484225631346));
#21708=CARTESIAN_POINT('Ctrl Pts',(142.748007567654,-5.67710331707251,333.333138131163));
#21709=CARTESIAN_POINT('Ctrl Pts',(142.755410134828,-5.63277533354574,333.182163088165));
#21710=CARTESIAN_POINT('Ctrl Pts',(142.762812702002,-5.58238628744325,333.032840274525));
#21711=CARTESIAN_POINT('Ctrl Pts',(142.770215269176,-5.52608515283655,332.885688422654));
#21712=CARTESIAN_POINT('Ctrl Pts',(142.77761393893,-5.4698136605311,332.73861404559));
#21713=CARTESIAN_POINT('Ctrl Pts',(142.785012608685,-5.40763641185448,332.593708701631));
#21714=CARTESIAN_POINT('Ctrl Pts',(142.79241127844,-5.33975183122995,332.451474751277));
#21715=CARTESIAN_POINT('Ctrl Pts',(142.799808727644,-5.27187844945332,332.309264265109));
#21716=CARTESIAN_POINT('Ctrl Pts',(142.807206176848,-5.19829976496392,332.169724634393));
#21717=CARTESIAN_POINT('Ctrl Pts',(142.814603626052,-5.11926187923096,332.033337165374));
#21718=CARTESIAN_POINT('Ctrl Pts',(142.822000754515,-5.04022742044303,331.896955609878));
#21719=CARTESIAN_POINT('Ctrl Pts',(142.829397882979,-4.95573441818043,331.763726267237));
#21720=CARTESIAN_POINT('Ctrl Pts',(142.836795011442,-4.86607423608487,331.634104563209));
#21721=CARTESIAN_POINT('Ctrl Pts',(142.844193278879,-4.7764002485594,331.504462900674));
#21722=CARTESIAN_POINT('Ctrl Pts',(142.851591546316,-4.68155770934711,331.378430289754));
#21723=CARTESIAN_POINT('Ctrl Pts',(142.858989813752,-4.58188039583534,331.2564318357));
#21724=CARTESIAN_POINT('Ctrl Pts',(142.866390680278,-4.48216806463516,331.134390522307));
#21725=CARTESIAN_POINT('Ctrl Pts',(142.873791546804,-4.37761781339542,331.016386476335));
#21726=CARTESIAN_POINT('Ctrl Pts',(142.88119241333,-4.26860253927908,330.90281036268));
#21727=CARTESIAN_POINT('Ctrl Pts',(142.888601406714,-4.15946755596934,330.789109531594));
#21728=CARTESIAN_POINT('Ctrl Pts',(142.896010400099,-4.04585801677911,330.679846612496));
#21729=CARTESIAN_POINT('Ctrl Pts',(142.903419393484,-3.92818291728981,330.575374645146));
#21730=CARTESIAN_POINT('Ctrl Pts',(142.910832951064,-3.81043532588013,330.470838319462));
#21731=CARTESIAN_POINT('Ctrl Pts',(142.918246508644,-3.68861747166693,330.371099062443));
#21732=CARTESIAN_POINT('Ctrl Pts',(142.925660066225,-3.56316958758489,330.276468159035));
#21733=CARTESIAN_POINT('Ctrl Pts',(142.933084178361,-3.4375431054737,330.181702531211));
#21734=CARTESIAN_POINT('Ctrl Pts',(142.940508290498,-3.30827657779703,330.092059994091));
#21735=CARTESIAN_POINT('Ctrl Pts',(142.947932402635,-3.1758379056566,330.007807680037));
#21736=CARTESIAN_POINT('Ctrl Pts',(142.951789527789,-3.10703068341109,329.964035210832));
#21737=CARTESIAN_POINT('Ctrl Pts',(142.955646652944,-3.03736762239442,329.921716917943));
#21738=CARTESIAN_POINT('Ctrl Pts',(142.959503778099,-2.96691662174357,329.880885201314));
#21739=CARTESIAN_POINT('Ctrl Pts',(142.966927755537,-2.8313165003209,329.802294610952));
#21740=CARTESIAN_POINT('Ctrl Pts',(142.974351732975,-2.69238698629703,329.728977046614));
#21741=CARTESIAN_POINT('Ctrl Pts',(142.981775710413,-2.55057677724521,329.661227794157));
#21742=CARTESIAN_POINT('Ctrl Pts',(142.98919092644,-2.40893392557663,329.593558496012));
#21743=CARTESIAN_POINT('Ctrl Pts',(142.996606142468,-2.26441747942392,329.531444588498));
#21744=CARTESIAN_POINT('Ctrl Pts',(143.004021358496,-2.11750349251186,329.47513714906));
#21745=CARTESIAN_POINT('Ctrl Pts',(143.01142943964,-1.97073086549829,329.418883888356));
#21746=CARTESIAN_POINT('Ctrl Pts',(143.018837520784,-1.82156563649957,329.368426105816));
#21747=CARTESIAN_POINT('Ctrl Pts',(143.026245601928,-1.67050665054391,329.323968103244));
#21748=CARTESIAN_POINT('Ctrl Pts',(143.033648169102,-1.51956010055028,329.279543191576));
#21749=CARTESIAN_POINT('Ctrl Pts',(143.041050736276,-1.36672295672868,329.241109272844));
#21750=CARTESIAN_POINT('Ctrl Pts',(143.04845330345,-1.21251205064942,329.208821787449));
#21751=CARTESIAN_POINT('Ctrl Pts',(143.055851973205,-1.05838233593813,329.176551301273));
#21752=CARTESIAN_POINT('Ctrl Pts',(143.06325064296,-0.902880663794444,329.150420879895));
#21753=CARTESIAN_POINT('Ctrl Pts',(143.070649312714,-0.746536858721354,
329.130535520078));
#21754=CARTESIAN_POINT('Ctrl Pts',(143.078046761918,-0.590218845521367,
329.110653440727));
#21755=CARTESIAN_POINT('Ctrl Pts',(143.085444211122,-0.433059344983441,
329.097014425284));
#21756=CARTESIAN_POINT('Ctrl Pts',(143.092841660326,-0.275596277423134,
329.089671984198));
#21757=CARTESIAN_POINT('Ctrl Pts',(143.10023878879,-0.118140037187029,329.082329861468));
#21758=CARTESIAN_POINT('Ctrl Pts',(143.107635917253,0.0396193710945745,
329.081283787649));
#21759=CARTESIAN_POINT('Ctrl Pts',(143.115033045717,0.197141296601919,329.086535205848));
#21760=CARTESIAN_POINT('Ctrl Pts',(143.122431313153,0.354687476553515,329.091787432634));
#21761=CARTESIAN_POINT('Ctrl Pts',(143.12982958059,0.51199572789554,329.103339069716));
#21762=CARTESIAN_POINT('Ctrl Pts',(143.137227848026,0.66852794445636,329.121139485412));
#21763=CARTESIAN_POINT('Ctrl Pts',(143.144628714552,0.825115152431099,329.138946154581));
#21764=CARTESIAN_POINT('Ctrl Pts',(143.152029581078,0.980925412232693,329.163005930985));
#21765=CARTESIAN_POINT('Ctrl Pts',(143.159430447604,1.13542840936469,329.193216648633));
#21766=CARTESIAN_POINT('Ctrl Pts',(143.166839440988,1.29010106555872,329.223460540538));
#21767=CARTESIAN_POINT('Ctrl Pts',(143.174248434373,1.44346322582083,329.259868790768));
#21768=CARTESIAN_POINT('Ctrl Pts',(143.181657427758,1.59499668050585,329.302288516283));
#21769=CARTESIAN_POINT('Ctrl Pts',(143.189070985338,1.74662348502579,329.344734373813));
#21770=CARTESIAN_POINT('Ctrl Pts',(143.196484542918,1.89641898491813,329.393198971281));
#21771=CARTESIAN_POINT('Ctrl Pts',(143.203898100499,2.04388317873062,329.447480561565));
#21772=CARTESIAN_POINT('Ctrl Pts',(143.211322212635,2.19155731481988,329.50183943163));
#21773=CARTESIAN_POINT('Ctrl Pts',(143.218746324772,2.33689317216164,329.56203169201));
#21774=CARTESIAN_POINT('Ctrl Pts',(143.226170436909,2.47941290531834,329.627808435337));
#21775=CARTESIAN_POINT('Ctrl Pts',(143.230027562063,2.55345764463177,329.66198210171));
#21776=CARTESIAN_POINT('Ctrl Pts',(143.233884687218,2.62674267952514,329.697662399409));
#21777=CARTESIAN_POINT('Ctrl Pts',(143.237741812373,2.69920402007419,329.734809764072));
#21778=CARTESIAN_POINT('Ctrl Pts',(143.245165789811,2.83867353060131,329.806308921106));
#21779=CARTESIAN_POINT('Ctrl Pts',(143.252589767249,2.97551056642688,329.883461372355));
#21780=CARTESIAN_POINT('Ctrl Pts',(143.260013744687,3.10922399937078,329.966049594579));
#21781=CARTESIAN_POINT('Ctrl Pts',(143.267428960714,3.24277963034558,330.048540350275));
#21782=CARTESIAN_POINT('Ctrl Pts',(143.274844176742,3.37321868168104,330.136453913517));
#21783=CARTESIAN_POINT('Ctrl Pts',(143.282259392769,3.50007239701229,330.229525832983));
#21784=CARTESIAN_POINT('Ctrl Pts',(143.289667473914,3.62680405433742,330.322508199118));
#21785=CARTESIAN_POINT('Ctrl Pts',(143.297075555058,3.74995694465513,330.420638821084));
#21786=CARTESIAN_POINT('Ctrl Pts',(143.304483636202,3.86908931255105,330.523608768885));
#21787=CARTESIAN_POINT('Ctrl Pts',(143.311886203376,3.98813300804967,330.626502074273));
#21788=CARTESIAN_POINT('Ctrl Pts',(143.31928877055,4.1031618585777,330.734227290387));
#21789=CARTESIAN_POINT('Ctrl Pts',(143.326691337724,4.2137654637697,330.846433920251));
#21790=CARTESIAN_POINT('Ctrl Pts',(143.334090007479,4.32431083664691,330.958581473815));
#21791=CARTESIAN_POINT('Ctrl Pts',(143.341488677233,4.43043534293211,331.075205477032));
#21792=CARTESIAN_POINT('Ctrl Pts',(143.348887346988,4.53176397016878,331.195917208948));
#21793=CARTESIAN_POINT('Ctrl Pts',(143.356284796192,4.63307588132849,331.316609027176));
#21794=CARTESIAN_POINT('Ctrl Pts',(143.363682245396,4.72959324394162,331.441386950166));
#21795=CARTESIAN_POINT('Ctrl Pts',(143.3710796946,4.82097996038017,331.569827586824));
#21796=CARTESIAN_POINT('Ctrl Pts',(143.378476823063,4.91236271444998,331.69826265452));
#21797=CARTESIAN_POINT('Ctrl Pts',(143.385873951527,4.99861504829554,331.830359816026));
#21798=CARTESIAN_POINT('Ctrl Pts',(143.39327107999,5.07944317119631,331.965665207482));
#21799=CARTESIAN_POINT('Ctrl Pts',(143.400669347427,5.16028373961033,332.10099143259));
#21800=CARTESIAN_POINT('Ctrl Pts',(143.408067614864,5.23569824269158,332.239526550826));
#21801=CARTESIAN_POINT('Ctrl Pts',(143.4154658823,5.3054380575754,332.380790657521));
#21802=CARTESIAN_POINT('Ctrl Pts',(143.422866748826,5.37520237278961,332.522104391782));
#21803=CARTESIAN_POINT('Ctrl Pts',(143.430267615352,5.43928786548871,332.666148688877));
#21804=CARTESIAN_POINT('Ctrl Pts',(143.437668481877,5.49749346562875,332.812422308152));
#21805=CARTESIAN_POINT('Ctrl Pts',(143.445077475262,5.55576298108242,332.958856549846));
#21806=CARTESIAN_POINT('Ctrl Pts',(143.452486468647,5.60813957156559,333.107524655552));
#21807=CARTESIAN_POINT('Ctrl Pts',(143.459895462032,5.65447136671199,333.257908117941));
#21808=CARTESIAN_POINT('Ctrl Pts',(143.467309019612,5.70083170384236,333.408384221731));
#21809=CARTESIAN_POINT('Ctrl Pts',(143.474722577192,5.74113973014074,333.560577427925));
#21810=CARTESIAN_POINT('Ctrl Pts',(143.482136134772,5.77529451959006,333.713958097692));
#21811=CARTESIAN_POINT('Ctrl Pts',(143.489560246909,5.80949793463501,333.867557132922));
#21812=CARTESIAN_POINT('Ctrl Pts',(143.496984359046,5.83753055051313,334.022346641888));
#21813=CARTESIAN_POINT('Ctrl Pts',(143.504408471183,5.85934308915607,334.177790096107));
#21814=CARTESIAN_POINT('Ctrl Pts',(143.508265596337,5.87067558116844,334.258549228832));
#21815=CARTESIAN_POINT('Ctrl Pts',(143.512122721492,5.88032999510254,334.339484834562));
#21816=CARTESIAN_POINT('Ctrl Pts',(143.515979846647,5.88830497285585,334.42052169226));
#21817=CARTESIAN_POINT('Ctrl Pts',(143.523403824085,5.90365476124339,334.576496875606));
#21818=CARTESIAN_POINT('Ctrl Pts',(143.530827801523,5.91282599080499,334.7333176767));
#21819=CARTESIAN_POINT('Ctrl Pts',(143.538251778961,5.91573580383548,334.89045338107));
#21820=CARTESIAN_POINT('Ctrl Pts',(143.545666994988,5.91864218284879,335.047403641667));
#21821=CARTESIAN_POINT('Ctrl Pts',(143.553082211016,5.91530184723368,335.20466769628));
#21822=CARTESIAN_POINT('Ctrl Pts',(143.560497427044,5.90568350878237,335.361708247896));
#21823=CARTESIAN_POINT('Ctrl Pts',(143.567905508188,5.89607442504789,335.518597695884));
#21824=CARTESIAN_POINT('Ctrl Pts',(143.575313589332,5.88019938697362,335.675263698984));
#21825=CARTESIAN_POINT('Ctrl Pts',(143.582721670476,5.85807912118249,335.831167595895));
#21826=CARTESIAN_POINT('Ctrl Pts',(143.59012423765,5.83597531990917,335.986955450688));
#21827=CARTESIAN_POINT('Ctrl Pts',(143.597526804824,5.8076355988372,336.141981960841));
#21828=CARTESIAN_POINT('Ctrl Pts',(143.604929371998,5.77313260716383,336.295712337906));
#21829=CARTESIAN_POINT('Ctrl Pts',(143.612328041753,5.73864778116478,336.449361776599));
#21830=CARTESIAN_POINT('Ctrl Pts',(143.619726711507,5.6980062285689,336.601716078027));
#21831=CARTESIAN_POINT('Ctrl Pts',(143.627125381262,5.6513318923623,336.752249526999));
#21832=CARTESIAN_POINT('Ctrl Pts',(143.634522830466,5.60466525597187,336.902758142627));
#21833=CARTESIAN_POINT('Ctrl Pts',(143.64192027967,5.5519679215841,337.051446145841));
#21834=CARTESIAN_POINT('Ctrl Pts',(143.649317728874,5.49341404609098,337.197801783763));
#21835=CARTESIAN_POINT('Ctrl Pts',(143.656714857338,5.43486270939183,337.344151075959));
#21836=CARTESIAN_POINT('Ctrl Pts',(143.664111985801,5.37045547511358,337.488167857427));
#21837=CARTESIAN_POINT('Ctrl Pts',(143.671509114265,5.30041502004282,337.629359461505));
#21838=CARTESIAN_POINT('Ctrl Pts',(143.678907381701,5.2303637804904,337.770572805565));
#21839=CARTESIAN_POINT('Ctrl Pts',(143.686305649138,5.15467775894931,337.908959771725));
#21840=CARTESIAN_POINT('Ctrl Pts',(143.693703916574,5.07362597339506,338.04405158376));
#21841=CARTESIAN_POINT('Ctrl Pts',(143.7011047831,4.99254571349615,338.179190854969));
#21842=CARTESIAN_POINT('Ctrl Pts',(143.708505649626,4.906096128343,338.311032347402));
#21843=CARTESIAN_POINT('Ctrl Pts',(143.715906516152,4.81458991135569,338.43913572689));
#21844=CARTESIAN_POINT('Ctrl Pts',(143.723315509536,4.72298321179376,338.567379776136));
#21845=CARTESIAN_POINT('Ctrl Pts',(143.730724502921,4.62630900848876,338.691877211051));
#21846=CARTESIAN_POINT('Ctrl Pts',(143.738133496306,4.52492113954678,338.812219726535));
#21847=CARTESIAN_POINT('Ctrl Pts',(143.745547053886,4.42347081218027,338.93263637716));
#21848=CARTESIAN_POINT('Ctrl Pts',(143.752960611466,4.31730128409592,339.048892733124));
#21849=CARTESIAN_POINT('Ctrl Pts',(143.760374169047,4.20680332302805,339.160617305624));
#21850=CARTESIAN_POINT('Ctrl Pts',(143.767798281183,4.09614804788336,339.272500938507));
#21851=CARTESIAN_POINT('Ctrl Pts',(143.77522239332,3.98115230446707,339.37983964837));
#21852=CARTESIAN_POINT('Ctrl Pts',(143.782646505457,3.86224060383601,339.482301649887));
#21853=CARTESIAN_POINT('Ctrl Pts',(143.786503630611,3.80046118789527,339.535534784862));
#21854=CARTESIAN_POINT('Ctrl Pts',(143.790360755766,3.73762526770217,339.587452287851));
#21855=CARTESIAN_POINT('Ctrl Pts',(143.794217880921,3.67379536328656,339.638012310375));
#21856=CARTESIAN_POINT('Ctrl Pts',(143.801641858359,3.5509391552939,339.735327396466));
#21857=CARTESIAN_POINT('Ctrl Pts',(143.809065835797,3.42402827659011,339.827904412912));
#21858=CARTESIAN_POINT('Ctrl Pts',(143.816489813235,3.29346417723805,339.915386482846));
#21859=CARTESIAN_POINT('Ctrl Pts',(143.823905029262,3.1630541631676,340.002765310777));
#21860=CARTESIAN_POINT('Ctrl Pts',(143.83132024529,3.02899981729281,340.085060955055));
#21861=CARTESIAN_POINT('Ctrl Pts',(143.838735461318,2.89173603228946,340.161956342518));
#21862=CARTESIAN_POINT('Ctrl Pts',(143.846143542462,2.75460432180896,340.238777741626));
#21863=CARTESIAN_POINT('Ctrl Pts',(143.853551623606,2.6142696434686,340.3102090472));
#21864=CARTESIAN_POINT('Ctrl Pts',(143.86095970475,2.47119618541267,340.375976188164));
#21865=CARTESIAN_POINT('Ctrl Pts',(143.868362271924,2.32822921954471,340.441694377443));
#21866=CARTESIAN_POINT('Ctrl Pts',(143.875764839098,2.18252787060725,340.501756641455));
#21867=CARTESIAN_POINT('Ctrl Pts',(143.883167406272,2.03458116826425,340.555934667744));
#21868=CARTESIAN_POINT('Ctrl Pts',(143.890566076026,1.88671235921323,340.61008416954));
#21869=CARTESIAN_POINT('Ctrl Pts',(143.897964745781,1.73660090068536,340.658355475503));
#21870=CARTESIAN_POINT('Ctrl Pts',(143.905363415536,1.58475595046043,340.70056831728));
#21871=CARTESIAN_POINT('Ctrl Pts',(143.91276086474,1.43293604993725,340.742774195249));
#21872=CARTESIAN_POINT('Ctrl Pts',(143.920158313944,1.27938358450519,340.77892349277));
#21873=CARTESIAN_POINT('Ctrl Pts',(143.927555763148,1.124623144367,340.808885723239));
#21874=CARTESIAN_POINT('Ctrl Pts',(143.934952891611,0.969869414371734,340.838846654599));
#21875=CARTESIAN_POINT('Ctrl Pts',(143.942350020075,0.813908180217969,340.86262098136));
#21876=CARTESIAN_POINT('Ctrl Pts',(143.949747148538,0.657274238999061,340.880129346983));
#21877=CARTESIAN_POINT('Ctrl Pts',(143.957145415975,0.500616180063091,340.897640408457));
#21878=CARTESIAN_POINT('Ctrl Pts',(143.964543683411,0.3432855787443,340.908883546284));
#21879=CARTESIAN_POINT('Ctrl Pts',(143.971941950848,0.185822220032969,340.913831301706));
#21880=CARTESIAN_POINT('Ctrl Pts',(143.979342817374,0.0283035427879143,
340.918780795327));
#21881=CARTESIAN_POINT('Ctrl Pts',(143.986743683899,-0.129347611915808,
340.91743049147));
#21882=CARTESIAN_POINT('Ctrl Pts',(143.994144550425,-0.286591741330341,
340.909805050617));
#21883=CARTESIAN_POINT('Ctrl Pts',(144.00155354381,-0.444008539832157,340.902171236302));
#21884=CARTESIAN_POINT('Ctrl Pts',(144.008962537195,-0.601017047460843,
340.888248541983));
#21885=CARTESIAN_POINT('Ctrl Pts',(144.016371530579,-0.757082429645215,
340.868113560355));
#21886=CARTESIAN_POINT('Ctrl Pts',(144.02378508816,-0.913243953488337,340.847966174884));
#21887=CARTESIAN_POINT('Ctrl Pts',(144.03119864574,-1.06846082709166,340.821598938691));
#21888=CARTESIAN_POINT('Ctrl Pts',(144.03861220332,-1.22220919075155,340.789139422794));
#21889=CARTESIAN_POINT('Ctrl Pts',(144.046036315457,-1.3761764433544,340.756633694832));
#21890=CARTESIAN_POINT('Ctrl Pts',(144.053460427593,-1.528670649666,340.718018455868));
#21891=CARTESIAN_POINT('Ctrl Pts',(144.06088453973,-1.67918307703539,340.673471138227));
#21892=CARTESIAN_POINT('Ctrl Pts',(144.064741664885,-1.75738034278653,340.650327013207));
#21893=CARTESIAN_POINT('Ctrl Pts',(144.06859879004,-1.83504300060573,340.625582487263));
#21894=CARTESIAN_POINT('Ctrl Pts',(144.072455915194,-1.91210202603938,340.599267488209));
#21895=CARTESIAN_POINT('Ctrl Pts',(144.079879892632,-2.06042090169271,340.548617858908));
#21896=CARTESIAN_POINT('Ctrl Pts',(144.08730387007,-2.20694964847762,340.491994529147));
#21897=CARTESIAN_POINT('Ctrl Pts',(144.094727847508,-2.35117091336048,340.429541960301));
#21898=CARTESIAN_POINT('Ctrl Pts',(144.102143063536,-2.49522197545173,340.367163094882));
#21899=CARTESIAN_POINT('Ctrl Pts',(144.109558279564,-2.63697063701664,340.298968830754));
#21900=CARTESIAN_POINT('Ctrl Pts',(144.116973495591,-2.77591491908541,340.225153291962));
#21901=CARTESIAN_POINT('Ctrl Pts',(144.124381576735,-2.91472550966543,340.15140877811));
#21902=CARTESIAN_POINT('Ctrl Pts',(144.131789657879,-3.0507367652961,340.072053931358));
#21903=CARTESIAN_POINT('Ctrl Pts',(144.139197739024,-3.18346701492038,339.987330781832));
#21904=CARTESIAN_POINT('Ctrl Pts',(144.146600306198,-3.31609847099563,339.902670693295));
#21905=CARTESIAN_POINT('Ctrl Pts',(144.154002873372,-3.44545347042777,339.812650458));
#21906=CARTESIAN_POINT('Ctrl Pts',(144.161405440546,-3.5710753783907,339.717557758454));
#21907=CARTESIAN_POINT('Ctrl Pts',(144.1688041103,-3.69663114696838,339.622515124799));
#21908=CARTESIAN_POINT('Ctrl Pts',(144.176202780055,-3.81845744157945,339.522405570298));
#21909=CARTESIAN_POINT('Ctrl Pts',(144.18360144981,-3.9361271362298,339.417559703041));
#21910=CARTESIAN_POINT('Ctrl Pts',(144.190998899014,-4.05377741903429,339.312731132097));
#21911=CARTESIAN_POINT('Ctrl Pts',(144.198396348218,-4.16727218441492,339.203168047151));
#21912=CARTESIAN_POINT('Ctrl Pts',(144.205793797422,-4.27621781754429,339.089240973508));
#21913=CARTESIAN_POINT('Ctrl Pts',(144.213190925885,-4.38515872698083,338.975318839545));
#21914=CARTESIAN_POINT('Ctrl Pts',(144.220588054349,-4.48955063841171,338.857033362838));
#21915=CARTESIAN_POINT('Ctrl Pts',(144.227985182812,-4.58903740983581,338.734791321296));
#21916=CARTESIAN_POINT('Ctrl Pts',(144.235383450249,-4.68853949973932,338.612530457531));
#21917=CARTESIAN_POINT('Ctrl Pts',(144.242781717685,-4.78313471020176,338.486312105389));
#21918=CARTESIAN_POINT('Ctrl Pts',(144.250179985122,-4.87250784193644,338.356575322076));
#21919=CARTESIAN_POINT('Ctrl Pts',(144.257580851648,-4.96191237139198,338.226792960866));
#21920=CARTESIAN_POINT('Ctrl Pts',(144.264981718174,-5.04609095790214,338.093490014637));
#21921=CARTESIAN_POINT('Ctrl Pts',(144.272382584699,-5.12477238309994,337.957133507963));
#21922=CARTESIAN_POINT('Ctrl Pts',(144.279791578084,-5.20354020802499,337.820627268807));
#21923=CARTESIAN_POINT('Ctrl Pts',(144.287200571469,-5.27679862996858,337.681061096332));
#21924=CARTESIAN_POINT('Ctrl Pts',(144.294609564854,-5.34432262768628,337.538926193039));
#21925=CARTESIAN_POINT('Ctrl Pts',(144.302023122434,-5.41188822251574,337.396703729743));
#21926=CARTESIAN_POINT('Ctrl Pts',(144.309436680014,-5.47371220772978,337.251909724867));
#21927=CARTESIAN_POINT('Ctrl Pts',(144.316850237595,-5.5296183699733,337.105053739208));
#21928=CARTESIAN_POINT('Ctrl Pts',(144.324274349731,-5.58560412487372,336.957988677168));
#21929=CARTESIAN_POINT('Ctrl Pts',(144.331698461868,-5.63565511175932,336.808856124213));
#21930=CARTESIAN_POINT('Ctrl Pts',(144.339122574005,-5.67964523282997,336.658179903295));
#21931=CARTESIAN_POINT('Ctrl Pts',(144.342979699159,-5.70249987179603,336.579897540209));
#21932=CARTESIAN_POINT('Ctrl Pts',(144.346836824314,-5.72371939245442,336.501198671567));
#21933=CARTESIAN_POINT('Ctrl Pts',(144.350693949468,-5.74329160865003,336.422157537163));
#21934=CARTESIAN_POINT('Ctrl Pts',(144.360547443046,-5.79329120650338,336.220237381848));
#21935=CARTESIAN_POINT('Ctrl Pts',(144.370400936624,-5.83266066500019,336.015588525642));
#21936=CARTESIAN_POINT('Ctrl Pts',(144.380254430202,-5.8611578583291,335.809171874355));
#21937=CARTESIAN_POINT('Ctrl Pts',(144.389879845096,-5.88899542750374,335.607533146545));
#21938=CARTESIAN_POINT('Ctrl Pts',(144.399505259989,-5.90645829256422,335.40420720989));
#21939=CARTESIAN_POINT('Ctrl Pts',(144.409130674883,-5.91336500329359,335.200112219323));
#21940=CARTESIAN_POINT('Ctrl Pts',(144.412187650663,-5.91555853444581,335.135292837514));
#21941=CARTESIAN_POINT('Ctrl Pts',(144.415244626444,-5.91668764623935,335.070396075559));
#21942=CARTESIAN_POINT('Ctrl Pts',(144.418301602224,-5.91674748820401,335.005451910815));
#21943=CARTESIAN_POINT('',(146.168301649435,-5.91279607591744,334.998941304638));
#21944=CARTESIAN_POINT('Ctrl Pts',(144.418301620294,-5.91612998447623,335.005450957973));
#21945=CARTESIAN_POINT('Ctrl Pts',(144.488511741443,-5.90248000309968,333.51400828609));
#21946=CARTESIAN_POINT('Ctrl Pts',(144.651467874018,-4.57331437570988,330.03073686821));
#21947=CARTESIAN_POINT('Ctrl Pts',(144.907170018015,1.28310118904558,328.122044325536));
#21948=CARTESIAN_POINT('Ctrl Pts',(145.18540805229,6.47817933912946,332.356930691166));
#21949=CARTESIAN_POINT('Ctrl Pts',(145.463646086563,5.72832792746371,339.017322749874));
#21950=CARTESIAN_POINT('Ctrl Pts',(145.741884120838,-0.27832547325347,341.991077016609));
#21951=CARTESIAN_POINT('Ctrl Pts',(145.976769298748,-5.1334511087582,339.085505629792));
#21952=CARTESIAN_POINT('Ctrl Pts',(146.118908465233,-5.90546254146294,336.052211088219));
#21953=CARTESIAN_POINT('Ctrl Pts',(146.168301620294,-5.90713908955371,334.998942939345));
#21954=CARTESIAN_POINT('',(147.918301620294,-5.91753216870106,334.994978908048));
#21955=CARTESIAN_POINT('Ctrl Pts',(146.168301669802,-5.91674990507826,334.998940162095));
#21956=CARTESIAN_POINT('Ctrl Pts',(146.176163441027,-5.91671982668063,334.831021695044));
#21957=CARTESIAN_POINT('Ctrl Pts',(146.184025212251,-5.9095371589622,334.663280561601));
#21958=CARTESIAN_POINT('Ctrl Pts',(146.191886983476,-5.89527254671868,334.496321369914));
#21959=CARTESIAN_POINT('Ctrl Pts',(146.19976273157,-5.88098257446191,334.329065353664));
#21960=CARTESIAN_POINT('Ctrl Pts',(146.207638479665,-5.85958553624748,334.162594350689));
#21961=CARTESIAN_POINT('Ctrl Pts',(146.215514227759,-5.83120336401502,333.997504169585));
#21962=CARTESIAN_POINT('Ctrl Pts',(146.223412142684,-5.80274130822188,333.831949330899));
#21963=CARTESIAN_POINT('Ctrl Pts',(146.231310057608,-5.76725484106339,333.667783381872));
#21964=CARTESIAN_POINT('Ctrl Pts',(146.239207972533,-5.72491673570582,333.50559077501));
#21965=CARTESIAN_POINT('Ctrl Pts',(146.24711774866,-5.68251504637494,333.343154584967));
#21966=CARTESIAN_POINT('Ctrl Pts',(146.255027524786,-5.63324125649986,333.182697938438));
#21967=CARTESIAN_POINT('Ctrl Pts',(146.262937300913,-5.5773170522976,333.024787337867));
#21968=CARTESIAN_POINT('Ctrl Pts',(146.270866048282,-5.52125871640332,332.866497995813));
#21969=CARTESIAN_POINT('Ctrl Pts',(146.278794795651,-5.45851817538879,332.710767188446));
#21970=CARTESIAN_POINT('Ctrl Pts',(146.286723543021,-5.38936493378601,332.558140836785));
#21971=CARTESIAN_POINT('Ctrl Pts',(146.290602425142,-5.35553395645441,332.483473351594));
#21972=CARTESIAN_POINT('Ctrl Pts',(146.294481307264,-5.3201688896589,332.409548469094));
#21973=CARTESIAN_POINT('Ctrl Pts',(146.298360189386,-5.28330512879898,332.336427684761));
#21974=CARTESIAN_POINT('Ctrl Pts',(146.305784166824,-5.2127498192254,332.196478329228));
#21975=CARTESIAN_POINT('Ctrl Pts',(146.313208144262,-5.13652356020408,332.059123196295));
#21976=CARTESIAN_POINT('Ctrl Pts',(146.3206321217,-5.0548405520916,331.92485487246));
#21977=CARTESIAN_POINT('Ctrl Pts',(146.328047337728,-4.97325394221863,331.79074500545));
#21978=CARTESIAN_POINT('Ctrl Pts',(146.335462553755,-4.8862235938338,331.659715012031));
#21979=CARTESIAN_POINT('Ctrl Pts',(146.342877769783,-4.79401078544132,331.532235424431));
#21980=CARTESIAN_POINT('Ctrl Pts',(146.350285850927,-4.70188670374885,331.404878497048));
#21981=CARTESIAN_POINT('Ctrl Pts',(146.357693932071,-4.60459030658873,331.281065474871));
#21982=CARTESIAN_POINT('Ctrl Pts',(146.365102013215,-4.50242753253622,331.161240190275));
#21983=CARTESIAN_POINT('Ctrl Pts',(146.372504580389,-4.40034080010215,331.041504093827));
#21984=CARTESIAN_POINT('Ctrl Pts',(146.379907147563,-4.29339514407098,330.925750107733));
#21985=CARTESIAN_POINT('Ctrl Pts',(146.387309714737,-4.18193828087265,330.814390990851));
#21986=CARTESIAN_POINT('Ctrl Pts',(146.394708384492,-4.07054009922543,330.703090504056));
#21987=CARTESIAN_POINT('Ctrl Pts',(146.402107054246,-3.95463570397611,330.596180541364));
#21988=CARTESIAN_POINT('Ctrl Pts',(146.409505724001,-3.83461127373347,330.494038732761));
#21989=CARTESIAN_POINT('Ctrl Pts',(146.416903173205,-3.71460664379512,330.391913774385));
#21990=CARTESIAN_POINT('Ctrl Pts',(146.424300622409,-3.59048361175089,330.294555650596));
#21991=CARTESIAN_POINT('Ctrl Pts',(146.431698071613,-3.46266328845441,330.202303311662));
#21992=CARTESIAN_POINT('Ctrl Pts',(146.439095200077,-3.33484850722429,330.110054972628));
#21993=CARTESIAN_POINT('Ctrl Pts',(146.44649232854,-3.20333705611192,330.022912196691));
#21994=CARTESIAN_POINT('Ctrl Pts',(146.453889457003,-3.06858080385524,329.94117183404));
#21995=CARTESIAN_POINT('Ctrl Pts',(146.46128772444,-2.93380380249963,329.859418885414));
#21996=CARTESIAN_POINT('Ctrl Pts',(146.468685991877,-2.79578132430925,329.783070199939));
#21997=CARTESIAN_POINT('Ctrl Pts',(146.476084259313,-2.65499158337609,329.712377636905));
#21998=CARTESIAN_POINT('Ctrl Pts',(146.483485125839,-2.51415238152651,329.64166023883));
#21999=CARTESIAN_POINT('Ctrl Pts',(146.490885992365,-2.37054431466596,329.576603086783));
#22000=CARTESIAN_POINT('Ctrl Pts',(146.49828685889,-2.22466725363737,329.517410632457));
#22001=CARTESIAN_POINT('Ctrl Pts',(146.505695852275,-2.07863000564912,329.458153179157));
#22002=CARTESIAN_POINT('Ctrl Pts',(146.51310484566,-1.93031913372141,329.404773425009));
#22003=CARTESIAN_POINT('Ctrl Pts',(146.520513839045,-1.78025210735936,329.357426739798));
#22004=CARTESIAN_POINT('Ctrl Pts',(146.527927396625,-1.63009263453265,329.310050887397));
#22005=CARTESIAN_POINT('Ctrl Pts',(146.535340954205,-1.47817521081658,329.268715607464));
#22006=CARTESIAN_POINT('Ctrl Pts',(146.542754511785,-1.32502878112974,329.233525401801));
#22007=CARTESIAN_POINT('Ctrl Pts',(146.550178623922,-1.17166431946315,329.198285096437));
#22008=CARTESIAN_POINT('Ctrl Pts',(146.557602736059,-1.01706772308561,329.169207406925));
#22009=CARTESIAN_POINT('Ctrl Pts',(146.565026848195,-0.861775175327489,
329.146345234839));
#22010=CARTESIAN_POINT('Ctrl Pts',(146.56888397335,-0.781094444583926,329.134467415994));
#22011=CARTESIAN_POINT('Ctrl Pts',(146.572741098505,-0.700225908248673,
329.124266444733));
#22012=CARTESIAN_POINT('Ctrl Pts',(146.57659822366,-0.619244776469927,329.115744187298));
#22013=CARTESIAN_POINT('Ctrl Pts',(146.584022201098,-0.463376851240116,
329.099341025779));
#22014=CARTESIAN_POINT('Ctrl Pts',(146.591446178536,-0.306621586995413,
329.08911056934));
#22015=CARTESIAN_POINT('Ctrl Pts',(146.598870155974,-0.14950912633372,329.08513925915));
#22016=CARTESIAN_POINT('Ctrl Pts',(146.606285372001,0.00741791798549277,
329.081172635704));
#22017=CARTESIAN_POINT('Ctrl Pts',(146.613700588029,0.16470095016472,329.083450464434));
#22018=CARTESIAN_POINT('Ctrl Pts',(146.621115804056,0.321802896826992,329.092007662658));
#22019=CARTESIAN_POINT('Ctrl Pts',(146.628523885201,0.47875368078709,329.100556627188));
#22020=CARTESIAN_POINT('Ctrl Pts',(146.635931966345,0.635523355940499,329.115372912598));
#22021=CARTESIAN_POINT('Ctrl Pts',(146.643340047489,0.791573133256018,329.136439431778));
#22022=CARTESIAN_POINT('Ctrl Pts',(146.650742614663,0.947506759872355,329.157490270763));
#22023=CARTESIAN_POINT('Ctrl Pts',(146.658145181837,1.10272118730054,329.184782030668));
#22024=CARTESIAN_POINT('Ctrl Pts',(146.665547749011,1.25668114849993,329.218245676829));
#22025=CARTESIAN_POINT('Ctrl Pts',(146.672946418765,1.41056005045274,329.251691704527));
#22026=CARTESIAN_POINT('Ctrl Pts',(146.68034508852,1.56318543776627,329.291303067899));
#22027=CARTESIAN_POINT('Ctrl Pts',(146.687743758275,1.71403076992517,329.336959378368));
#22028=CARTESIAN_POINT('Ctrl Pts',(146.695141207479,1.86485121728831,329.382608156964));
#22029=CARTESIAN_POINT('Ctrl Pts',(146.702538656683,2.01389183544407,329.434299795469));
#22030=CARTESIAN_POINT('Ctrl Pts',(146.709936105887,2.16063970663593,329.491863598221));
#22031=CARTESIAN_POINT('Ctrl Pts',(146.71733323435,2.30738121509588,329.549424905106));
#22032=CARTESIAN_POINT('Ctrl Pts',(146.724730362814,2.45182982681364,329.612857733709));
#22033=CARTESIAN_POINT('Ctrl Pts',(146.732127491277,2.59349138202934,329.681942740639));
#22034=CARTESIAN_POINT('Ctrl Pts',(146.739525758714,2.73517474958819,329.751038384936));
#22035=CARTESIAN_POINT('Ctrl Pts',(146.746924026151,2.87406987070856,329.82578777683));
#22036=CARTESIAN_POINT('Ctrl Pts',(146.754322293587,3.00970616245622,329.905925071402));
#22037=CARTESIAN_POINT('Ctrl Pts',(146.761723160113,3.14539010465955,329.986090519048));
#22038=CARTESIAN_POINT('Ctrl Pts',(146.769124026639,3.27781261695689,330.071647448264));
#22039=CARTESIAN_POINT('Ctrl Pts',(146.776524893164,3.40653126276212,330.162286147536));
#22040=CARTESIAN_POINT('Ctrl Pts',(146.783933886549,3.53539125394656,330.253024376765));
#22041=CARTESIAN_POINT('Ctrl Pts',(146.791342879934,3.66053895089339,330.348855305143));
#22042=CARTESIAN_POINT('Ctrl Pts',(146.798751873319,3.78156366739261,330.449427861031));
#22043=CARTESIAN_POINT('Ctrl Pts',(146.806165430899,3.90266293929173,330.550062373083));
#22044=CARTESIAN_POINT('Ctrl Pts',(146.813578988479,4.01963389302959,330.655444083913));
#22045=CARTESIAN_POINT('Ctrl Pts',(146.82099254606,4.1321024083657,330.765184744374));
#22046=CARTESIAN_POINT('Ctrl Pts',(146.828416658196,4.24473104322347,330.875081640757));
#22047=CARTESIAN_POINT('Ctrl Pts',(146.835840770333,4.35284418173045,330.989349610552));
#22048=CARTESIAN_POINT('Ctrl Pts',(146.84326488247,4.45610717825678,331.107566393837));
#22049=CARTESIAN_POINT('Ctrl Pts',(146.847122007624,4.50975646238894,331.168984772239));
#22050=CARTESIAN_POINT('Ctrl Pts',(146.850979132779,4.56209728199605,331.231468518815));
#22051=CARTESIAN_POINT('Ctrl Pts',(146.854836257934,4.61308736718765,331.294955397678));
#22052=CARTESIAN_POINT('Ctrl Pts',(146.862260235372,4.71123021369702,331.417151369389));
#22053=CARTESIAN_POINT('Ctrl Pts',(146.86968421281,4.80466249087155,331.543433928317));
#22054=CARTESIAN_POINT('Ctrl Pts',(146.877108190248,4.89302461790924,331.673404044517));
#22055=CARTESIAN_POINT('Ctrl Pts',(146.884523406275,4.98128246434223,331.803220776426));
#22056=CARTESIAN_POINT('Ctrl Pts',(146.891938622303,5.06448186317861,331.936716097499));
#22057=CARTESIAN_POINT('Ctrl Pts',(146.899353838331,5.1423028104795,332.073457267041));
#22058=CARTESIAN_POINT('Ctrl Pts',(146.906761919475,5.2200488788567,332.210066864918));
#22059=CARTESIAN_POINT('Ctrl Pts',(146.914170000619,5.29242661503159,332.349915771483));
#22060=CARTESIAN_POINT('Ctrl Pts',(146.921578081763,5.35915881825845,332.492541660728));
#22061=CARTESIAN_POINT('Ctrl Pts',(146.928980648937,5.4258413514877,332.63506139092));
#22062=CARTESIAN_POINT('Ctrl Pts',(146.936383216111,5.48688656122312,332.780353651584));
#22063=CARTESIAN_POINT('Ctrl Pts',(146.943785783285,5.54206283647608,332.92793096663));
#22064=CARTESIAN_POINT('Ctrl Pts',(146.95118445304,5.59721006166128,333.075430582865));
#22065=CARTESIAN_POINT('Ctrl Pts',(146.958583122794,5.64649437584844,333.225212508797));
#22066=CARTESIAN_POINT('Ctrl Pts',(146.965981792549,5.68973207507486,333.376768816106));
#22067=CARTESIAN_POINT('Ctrl Pts',(146.973379241753,5.73296264142352,333.528300121332));
#22068=CARTESIAN_POINT('Ctrl Pts',(146.980776690957,5.77014847024491,333.681604868442));
#22069=CARTESIAN_POINT('Ctrl Pts',(146.988174140161,5.80115553393411,333.836159360735));
#22070=CARTESIAN_POINT('Ctrl Pts',(146.995571268625,5.83216125321106,333.990707151814));
#22071=CARTESIAN_POINT('Ctrl Pts',(147.002968397088,5.85698866661858,334.146504214416));
#22072=CARTESIAN_POINT('Ctrl Pts',(147.010365525551,5.87555480649272,334.30301629976));
#22073=CARTESIAN_POINT('Ctrl Pts',(147.017763792988,5.89412380508894,334.459552484058));
#22074=CARTESIAN_POINT('Ctrl Pts',(147.025162060425,5.90642956657555,334.616803539679));
#22075=CARTESIAN_POINT('Ctrl Pts',(147.032560327861,5.91244098618906,334.774229879453));
#22076=CARTESIAN_POINT('Ctrl Pts',(147.039961194387,5.91845451767749,334.931711524756));
#22077=CARTESIAN_POINT('Ctrl Pts',(147.047362060913,5.91816929042905,335.089368204112));
#22078=CARTESIAN_POINT('Ctrl Pts',(147.054762927439,5.91160631963916,335.246660260485));
#22079=CARTESIAN_POINT('Ctrl Pts',(147.062171920823,5.9050361420799,335.404125038573));
#22080=CARTESIAN_POINT('Ctrl Pts',(147.069580914208,5.89217446973443,335.561224020968));
#22081=CARTESIAN_POINT('Ctrl Pts',(147.076989907593,5.87309428036108,335.717421867864));
#22082=CARTESIAN_POINT('Ctrl Pts',(147.084403465173,5.85400233693294,335.873715938022));
#22083=CARTESIAN_POINT('Ctrl Pts',(147.091817022753,5.82868430293561,336.029107399018));
#22084=CARTESIAN_POINT('Ctrl Pts',(147.099230580334,5.79726420742942,336.183071541268));
#22085=CARTESIAN_POINT('Ctrl Pts',(147.10665469247,5.76579937966508,336.337254879661));
#22086=CARTESIAN_POINT('Ctrl Pts',(147.114078804607,5.72821522884073,336.490006479475));
#22087=CARTESIAN_POINT('Ctrl Pts',(147.121502916744,5.68468574638215,336.640816420987));
#22088=CARTESIAN_POINT('Ctrl Pts',(147.125360041898,5.66207042771921,336.71916825731));
#22089=CARTESIAN_POINT('Ctrl Pts',(147.129217167053,5.63785113299624,336.796996309748));
#22090=CARTESIAN_POINT('Ctrl Pts',(147.133074292208,5.61205732303508,336.87423135324));
#22091=CARTESIAN_POINT('Ctrl Pts',(147.140498269646,5.56241084916839,337.022889018552));
#22092=CARTESIAN_POINT('Ctrl Pts',(147.147922247084,5.50677871756783,337.169796952446));
#22093=CARTESIAN_POINT('Ctrl Pts',(147.155346224522,5.44530189122188,337.314436837755));
#22094=CARTESIAN_POINT('Ctrl Pts',(147.162761440549,5.38389761678068,337.458906026237));
#22095=CARTESIAN_POINT('Ctrl Pts',(147.170176656577,5.31666252198309,337.601112153892));
#22096=CARTESIAN_POINT('Ctrl Pts',(147.177591872605,5.24378733521979,337.740551941761));
#22097=CARTESIAN_POINT('Ctrl Pts',(147.184999953749,5.17098226859426,337.879857561367));
#22098=CARTESIAN_POINT('Ctrl Pts',(147.192408034893,5.09254808559639,338.016401811699));
#22099=CARTESIAN_POINT('Ctrl Pts',(147.199816116037,5.00872355679883,338.149701397604));
#22100=CARTESIAN_POINT('Ctrl Pts',(147.207218683211,4.92496142012899,338.282901766193));
#22101=CARTESIAN_POINT('Ctrl Pts',(147.214621250385,4.83581712422319,338.412861964516));
#22102=CARTESIAN_POINT('Ctrl Pts',(147.222023817559,4.74157526013046,338.539123424666));
#22103=CARTESIAN_POINT('Ctrl Pts',(147.229422487314,4.64738301396727,338.665318408709));
#22104=CARTESIAN_POINT('Ctrl Pts',(147.236821157068,4.54809876733374,338.787818234551));
#22105=CARTESIAN_POINT('Ctrl Pts',(147.244219826823,4.44405023523495,338.906193552451));
#22106=CARTESIAN_POINT('Ctrl Pts',(147.251617276027,4.34001886791312,339.024549342099));
#22107=CARTESIAN_POINT('Ctrl Pts',(147.259014725231,4.23122502115273,339.138781694165));
#22108=CARTESIAN_POINT('Ctrl Pts',(147.266412174435,4.11803655265524,339.248494499643));
#22109=CARTESIAN_POINT('Ctrl Pts',(147.273809302899,4.00485299181242,339.358202548164));
#22110=CARTESIAN_POINT('Ctrl Pts',(147.281206431362,3.88727545607765,339.463391179976));
#22111=CARTESIAN_POINT('Ctrl Pts',(147.288603559826,3.76570830808351,339.563701513128));
#22112=CARTESIAN_POINT('Ctrl Pts',(147.296001827262,3.64412244178326,339.664027291568));
#22113=CARTESIAN_POINT('Ctrl Pts',(147.303400094699,3.51854602795255,339.759473038194));
#22114=CARTESIAN_POINT('Ctrl Pts',(147.310798362135,3.38941598438095,339.849720594769));
#22115=CARTESIAN_POINT('Ctrl Pts',(147.318199228661,3.26024057606695,339.939999856259));
#22116=CARTESIAN_POINT('Ctrl Pts',(147.325600095187,3.12750935810849,340.025077078118));
#22117=CARTESIAN_POINT('Ctrl Pts',(147.333000961713,2.9916875121479,340.104677893086));
#22118=CARTESIAN_POINT('Ctrl Pts',(147.340409955097,2.85571652081542,340.184366117358));
#22119=CARTESIAN_POINT('Ctrl Pts',(147.347818948482,2.71664844605113,340.258565736403));
#22120=CARTESIAN_POINT('Ctrl Pts',(147.355227941867,2.57497295897001,340.327048415687));
#22121=CARTESIAN_POINT('Ctrl Pts',(147.362641499447,2.4332101949019,340.395573282664));
#22122=CARTESIAN_POINT('Ctrl Pts',(147.370055057027,2.28883715927508,340.458374043644));
#22123=CARTESIAN_POINT('Ctrl Pts',(147.377468614608,2.14236221081269,340.515271046846));
#22124=CARTESIAN_POINT('Ctrl Pts',(147.384892726744,1.99567872844555,340.572249053349));
#22125=CARTESIAN_POINT('Ctrl Pts',(147.392316838881,1.84688770876028,340.623306394643));
#22126=CARTESIAN_POINT('Ctrl Pts',(147.399740951018,1.69651211087499,340.668313437007));
#22127=CARTESIAN_POINT('Ctrl Pts',(147.403598076172,1.61838593355299,340.691696407528));
#22128=CARTESIAN_POINT('Ctrl Pts',(147.407455201327,1.53983221379161,340.713447110847));
#22129=CARTESIAN_POINT('Ctrl Pts',(147.411312326482,1.46092510736363,340.733552859543));
#22130=CARTESIAN_POINT('Ctrl Pts',(147.41873630392,1.30904914940758,340.772251273183));
#22131=CARTESIAN_POINT('Ctrl Pts',(147.426160281358,1.15540539507283,340.804969339466));
#22132=CARTESIAN_POINT('Ctrl Pts',(147.433584258796,1.00050599148444,340.831545106016));
#22133=CARTESIAN_POINT('Ctrl Pts',(147.440999474823,0.845789392498042,340.858089509164));
#22134=CARTESIAN_POINT('Ctrl Pts',(147.448414690851,0.689820458173766,340.878505979011));
#22135=CARTESIAN_POINT('Ctrl Pts',(147.455829906879,0.533125620602867,340.892682550007));
#22136=CARTESIAN_POINT('Ctrl Pts',(147.463237988023,0.376581554015769,340.906845480377));
#22137=CARTESIAN_POINT('Ctrl Pts',(147.470646069167,0.219313343895595,340.914780431336));
#22138=CARTESIAN_POINT('Ctrl Pts',(147.478054150311,0.0618566159030756,
340.916426651415));
#22139=CARTESIAN_POINT('Ctrl Pts',(147.485456717485,-0.0954829141711237,
340.918071646181));
#22140=CARTESIAN_POINT('Ctrl Pts',(147.492859284659,-0.253010311133119,
340.913437226371));
#22141=CARTESIAN_POINT('Ctrl Pts',(147.500261851833,-0.410185946901329,
340.902514553262));
#22142=CARTESIAN_POINT('Ctrl Pts',(147.507660521588,-0.567278830384351,
340.891597630892));
#22143=CARTESIAN_POINT('Ctrl Pts',(147.515059191342,-0.724019950136165,
340.874399074563));
#22144=CARTESIAN_POINT('Ctrl Pts',(147.522457861097,-0.879870911407023,
340.850962121033));
#22145=CARTESIAN_POINT('Ctrl Pts',(147.529855310301,-1.03569616210859,340.827529033872));
#22146=CARTESIAN_POINT('Ctrl Pts',(147.537252759505,-1.19063117707332,340.797859647471));
#22147=CARTESIAN_POINT('Ctrl Pts',(147.544650208709,-1.34414379087642,340.762048943904));
#22148=CARTESIAN_POINT('Ctrl Pts',(147.552047337173,-1.49764974864022,340.726239793028));
#22149=CARTESIAN_POINT('Ctrl Pts',(147.559444465636,-1.6497330644151,340.684289939217));
#22150=CARTESIAN_POINT('Ctrl Pts',(147.5668415941,-1.79987312289148,340.636345208022));
#22151=CARTESIAN_POINT('Ctrl Pts',(147.574239861536,-1.95003629918897,340.588393094535));
#22152=CARTESIAN_POINT('Ctrl Pts',(147.581638128973,-2.09825526686946,340.534444379265));
#22153=CARTESIAN_POINT('Ctrl Pts',(147.589036396409,-2.24402603859688,340.474694302023));
#22154=CARTESIAN_POINT('Ctrl Pts',(147.596437262935,-2.38984802112968,340.41492323395));
#22155=CARTESIAN_POINT('Ctrl Pts',(147.603838129461,-2.53321975018744,340.34934688755));
#22156=CARTESIAN_POINT('Ctrl Pts',(147.611238995987,-2.67365876800804,340.278207968123));
#22157=CARTESIAN_POINT('Ctrl Pts',(147.618647989371,-2.81425200129645,340.206990931361));
#22158=CARTESIAN_POINT('Ctrl Pts',(147.626056982756,-2.95190575890977,340.130199291842));
#22159=CARTESIAN_POINT('Ctrl Pts',(147.633465976141,-3.08616304033104,340.048121259538));
#22160=CARTESIAN_POINT('Ctrl Pts',(147.640879533721,-3.22050302886869,339.965992664334));
#22161=CARTESIAN_POINT('Ctrl Pts',(147.648293091301,-3.3514420622727,339.878571393885));
#22162=CARTESIAN_POINT('Ctrl Pts',(147.655706648882,-3.47855396545394,339.786187717999));
#22163=CARTESIAN_POINT('Ctrl Pts',(147.663130761018,-3.60584683570027,339.693672517038));
#22164=CARTESIAN_POINT('Ctrl Pts',(147.670554873155,-3.72930140163319,339.59618103131));
#22165=CARTESIAN_POINT('Ctrl Pts',(147.677978985292,-3.84852564830608,339.494082876053));
#22166=CARTESIAN_POINT('Ctrl Pts',(147.681836110446,-3.91046744449855,339.441038773858));
#22167=CARTESIAN_POINT('Ctrl Pts',(147.685693235601,-3.97126800012368,339.386751828662));
#22168=CARTESIAN_POINT('Ctrl Pts',(147.689550360756,-4.0308765161159,339.331277533745));
#22169=CARTESIAN_POINT('Ctrl Pts',(147.696863948988,-4.14390166402496,339.226091382341));
#22170=CARTESIAN_POINT('Ctrl Pts',(147.70417753722,-4.25300172650221,339.116296409232));
#22171=CARTESIAN_POINT('Ctrl Pts',(147.711491125452,-4.35776915270144,339.002221704786));
#22172=CARTESIAN_POINT('Ctrl Pts',(147.718795981515,-4.46241149023985,338.888283201568));
#22173=CARTESIAN_POINT('Ctrl Pts',(147.726100837577,-4.56273122552003,338.77007541406));
#22174=CARTESIAN_POINT('Ctrl Pts',(147.73340569364,-4.65835459729738,338.647966969195));
#22175=CARTESIAN_POINT('Ctrl Pts',(147.740703533841,-4.75388612875338,338.525975801922));
#22176=CARTESIAN_POINT('Ctrl Pts',(147.748001374042,-4.84473003641664,338.400091733477));
#22177=CARTESIAN_POINT('Ctrl Pts',(147.755299214243,-4.93055029611225,338.270719238945));
#22178=CARTESIAN_POINT('Ctrl Pts',(147.762591395003,-5.01630400259889,338.141447072177));
#22179=CARTESIAN_POINT('Ctrl Pts',(147.769883575763,-5.09704160545529,338.008692185167));
#22180=CARTESIAN_POINT('Ctrl Pts',(147.777175756523,-5.17246839520712,337.872890750287));
#22181=CARTESIAN_POINT('Ctrl Pts',(147.784464896139,-5.24786372883292,337.737145950285));
#22182=CARTESIAN_POINT('Ctrl Pts',(147.791754035754,-5.3179524685946,337.598357465983));
#22183=CARTESIAN_POINT('Ctrl Pts',(147.79904317537,-5.38248419701184,337.456988895257));
#22184=CARTESIAN_POINT('Ctrl Pts',(147.806330812989,-5.44700262804597,337.315649454885));
#22185=CARTESIAN_POINT('Ctrl Pts',(147.813618450607,-5.50596616673139,337.171731336426));
#22186=CARTESIAN_POINT('Ctrl Pts',(147.820906088225,-5.55917132215087,337.025720803436));
#22187=CARTESIAN_POINT('Ctrl Pts',(147.828193761638,-5.61237673889338,336.8797095533));
#22188=CARTESIAN_POINT('Ctrl Pts',(147.83548143505,-5.65982358579274,336.731606230687));
#22189=CARTESIAN_POINT('Ctrl Pts',(147.842769108463,-5.70135740753455,336.581914749299));
#22190=CARTESIAN_POINT('Ctrl Pts',(147.85006117729,-5.74291627957087,336.432132984487));
#22191=CARTESIAN_POINT('Ctrl Pts',(147.857353246117,-5.77855490092662,336.280761519495));
#22192=CARTESIAN_POINT('Ctrl Pts',(147.864645314944,-5.80816929984917,336.128317307671));
#22193=CARTESIAN_POINT('Ctrl Pts',(147.871939876106,-5.83779382058973,335.975820992389));
#22194=CARTESIAN_POINT('Ctrl Pts',(147.879234437268,-5.86138995737384,335.822251580241));
#22195=CARTESIAN_POINT('Ctrl Pts',(147.886528998429,-5.87890541429882,335.668132989926));
#22196=CARTESIAN_POINT('Ctrl Pts',(147.893830941335,-5.8964385960224,335.513858439023));
#22197=CARTESIAN_POINT('Ctrl Pts',(147.901132884242,-5.90787878264885,335.359033983944));
#22198=CARTESIAN_POINT('Ctrl Pts',(147.908434827148,-5.91322574581222,335.204185801572));
#22199=CARTESIAN_POINT('Ctrl Pts',(147.911723758197,-5.9156341175826,335.134439296925));
#22200=CARTESIAN_POINT('Ctrl Pts',(147.915012689245,-5.91680701839214,335.064687952162));
#22201=CARTESIAN_POINT('Ctrl Pts',(147.918301620294,-5.9167478700565,334.994979573534));
#22202=CARTESIAN_POINT('',(149.668301620294,-5.92062882697594,335.003695392425));
#22203=CARTESIAN_POINT('Ctrl Pts',(147.918301620294,-5.92002000212284,334.994976797094));
#22204=CARTESIAN_POINT('Ctrl Pts',(147.934797211872,-5.92318185887226,334.645159030833));
#22205=CARTESIAN_POINT('Ctrl Pts',(148.044038814879,-5.735551808118,332.331887814483));
#22206=CARTESIAN_POINT('Ctrl Pts',(148.246026429301,-2.68677370757217,328.53982430846));
#22207=CARTESIAN_POINT('Ctrl Pts',(148.524264463577,3.97853214060743,329.244662918007));
#22208=CARTESIAN_POINT('Ctrl Pts',(148.80250249785,6.99279776638912,335.231089419058));
#22209=CARTESIAN_POINT('Ctrl Pts',(149.080740532125,3.58987609548163,341.005448571115));
#22210=CARTESIAN_POINT('Ctrl Pts',(149.358978566399,-3.10742188176739,341.268696209736));
#22211=CARTESIAN_POINT('Ctrl Pts',(149.554832262455,-5.81441077913725,337.404639393051));
#22212=CARTESIAN_POINT('Ctrl Pts',(149.657939947087,-5.92516035764709,335.223093199081));
#22213=CARTESIAN_POINT('Ctrl Pts',(149.668301620294,-5.92355705250644,335.003697220093));
#22214=CARTESIAN_POINT('',(151.4183015929,-5.9121545373304,335.003046556256));
#22215=CARTESIAN_POINT('Ctrl Pts',(149.668301620294,-5.91674884750632,335.003692970715));
#22216=CARTESIAN_POINT('Ctrl Pts',(149.67562186246,-5.91684547825825,334.848874551005));
#22217=CARTESIAN_POINT('Ctrl Pts',(149.682942104626,-5.91086145436701,334.693814183029));
#22218=CARTESIAN_POINT('Ctrl Pts',(149.690262346792,-5.89876627030689,334.53903682274));
#22219=CARTESIAN_POINT('Ctrl Pts',(149.697574904694,-5.88668378290076,334.384421936587));
#22220=CARTESIAN_POINT('Ctrl Pts',(149.704887462596,-5.86850292911253,334.230089846584));
#22221=CARTESIAN_POINT('Ctrl Pts',(149.712200020498,-5.84424520377401,334.076566970125));
#22222=CARTESIAN_POINT('Ctrl Pts',(149.719506597661,-5.82000731816153,333.923169655801));
#22223=CARTESIAN_POINT('Ctrl Pts',(149.726813174823,-5.78970251150662,333.7705806152));
#22224=CARTESIAN_POINT('Ctrl Pts',(149.734119751986,-5.75340418977252,333.619322343337));
#22225=CARTESIAN_POINT('Ctrl Pts',(149.741675372109,-5.7158686482948,333.462908468917));
#22226=CARTESIAN_POINT('Ctrl Pts',(149.749230992232,-5.67192379597278,333.307918107546));
#22227=CARTESIAN_POINT('Ctrl Pts',(149.756786612356,-5.62170869794327,333.15491954702));
#22228=CARTESIAN_POINT('Ctrl Pts',(149.764087191177,-5.57318861948603,333.007085480138));
#22229=CARTESIAN_POINT('Ctrl Pts',(149.771387769998,-5.51881485905228,332.861111323308));
#22230=CARTESIAN_POINT('Ctrl Pts',(149.778688348819,-5.45876389216768,332.717495381808));
#22231=CARTESIAN_POINT('Ctrl Pts',(149.785988453333,-5.3987168267073,332.573888770828));
#22232=CARTESIAN_POINT('Ctrl Pts',(149.793288557846,-5.33299343645006,332.432640424818));
#22233=CARTESIAN_POINT('Ctrl Pts',(149.800588662359,-5.26181845823944,332.294228931519));
#22234=CARTESIAN_POINT('Ctrl Pts',(149.807889823491,-5.190633178144,332.155797404504));
#22235=CARTESIAN_POINT('Ctrl Pts',(149.815190984623,-5.11399491584785,332.020203888682));
#22236=CARTESIAN_POINT('Ctrl Pts',(149.822492145756,-5.03217435700199,331.887902346771));
#22237=CARTESIAN_POINT('Ctrl Pts',(149.82979589504,-4.9503247939981,331.755553905953));
#22238=CARTESIAN_POINT('Ctrl Pts',(149.837099644324,-4.8632894812332,331.626500087206));
#22239=CARTESIAN_POINT('Ctrl Pts',(149.844403393608,-4.77138222962384,331.501165596755));
#22240=CARTESIAN_POINT('Ctrl Pts',(149.851714988852,-4.679376247809,331.375696467309));
#22241=CARTESIAN_POINT('Ctrl Pts',(149.859026584097,-4.58248810750462,331.25395495101));
#22242=CARTESIAN_POINT('Ctrl Pts',(149.866338179341,-4.48107199398705,331.136332785137));
#22243=CARTESIAN_POINT('Ctrl Pts',(149.873654464745,-4.37959082521267,331.018635168334));
#22244=CARTESIAN_POINT('Ctrl Pts',(149.880970750149,-4.27357616084882,330.905062443029));
#22245=CARTESIAN_POINT('Ctrl Pts',(149.888287035552,-4.1634181836864,330.795968650182));
#22246=CARTESIAN_POINT('Ctrl Pts',(149.895613120946,-4.05311265254148,330.686728728803));
#22247=CARTESIAN_POINT('Ctrl Pts',(149.902939206339,-3.93865301503498,330.581979969939));
#22248=CARTESIAN_POINT('Ctrl Pts',(149.910265291733,-3.82046190193295,330.482035699745));
#22249=CARTESIAN_POINT('Ctrl Pts',(149.911995072804,-3.79255549090281,330.458437598238));
#22250=CARTESIAN_POINT('Ctrl Pts',(149.913724853875,-3.76444117656519,330.435107150208));
#22251=CARTESIAN_POINT('Ctrl Pts',(149.915454634946,-3.73612474250915,330.412048118069));
#22252=CARTESIAN_POINT('Ctrl Pts',(149.922878612384,-3.61459458412496,330.313081990397));
#22253=CARTESIAN_POINT('Ctrl Pts',(149.930302589822,-3.48894610853022,330.218798716758));
#22254=CARTESIAN_POINT('Ctrl Pts',(149.93772656726,-3.3595759073391,330.12956056548));
#22255=CARTESIAN_POINT('Ctrl Pts',(149.945141783288,-3.23035838245033,330.040427728647));
#22256=CARTESIAN_POINT('Ctrl Pts',(149.952556999316,-3.0974281789271,329.956328372487));
#22257=CARTESIAN_POINT('Ctrl Pts',(149.959972215343,-2.96121586573633,329.877585417109));
#22258=CARTESIAN_POINT('Ctrl Pts',(149.967380296487,-2.82513461534728,329.798918227806));
#22259=CARTESIAN_POINT('Ctrl Pts',(149.974788377631,-2.68577786328597,329.725597364363));
#22260=CARTESIAN_POINT('Ctrl Pts',(149.982196458776,-2.54360605231989,329.657903144541));
#22261=CARTESIAN_POINT('Ctrl Pts',(149.98959902595,-2.40154006242959,329.590259310764));
#22262=CARTESIAN_POINT('Ctrl Pts',(149.997001593124,-2.25666352120201,329.528233941419));
#22263=CARTESIAN_POINT('Ctrl Pts',(150.004404160298,-2.10946232890685,329.472061935457));
#22264=CARTESIAN_POINT('Ctrl Pts',(150.011802830052,-1.96233863739557,329.415919503811));
#22265=CARTESIAN_POINT('Ctrl Pts',(150.019201499807,-1.81289308013125,329.365624430744));
#22266=CARTESIAN_POINT('Ctrl Pts',(150.026600169562,-1.66163233279155,329.321363847443));
#22267=CARTESIAN_POINT('Ctrl Pts',(150.033997618766,-1.51039653877853,329.277110565765));
#22268=CARTESIAN_POINT('Ctrl Pts',(150.04139506797,-1.35734650684511,329.23888990281));
#22269=CARTESIAN_POINT('Ctrl Pts',(150.048792517174,-1.20300501629026,329.206839421069));
#22270=CARTESIAN_POINT('Ctrl Pts',(150.056189645637,-1.04867021771348,329.174790328981));
#22271=CARTESIAN_POINT('Ctrl Pts',(150.063586774101,-0.89304443726818,329.148910962054));
#22272=CARTESIAN_POINT('Ctrl Pts',(150.070983902564,-0.736661351036444,
329.12928789529));
#22273=CARTESIAN_POINT('Ctrl Pts',(150.078382170001,-0.580254185713053,
329.109661807064));
#22274=CARTESIAN_POINT('Ctrl Pts',(150.085780437438,-0.423089852754835,
329.096293983554));
#22275=CARTESIAN_POINT('Ctrl Pts',(150.093178704874,-0.265707716882427,
329.089219174112));
#22276=CARTESIAN_POINT('Ctrl Pts',(150.1005795714,-0.1082702910109,329.082141879214));
#22277=CARTESIAN_POINT('Ctrl Pts',(150.107980437926,0.0493847175190642,
329.081362016835));
#22278=CARTESIAN_POINT('Ctrl Pts',(150.115381304451,0.206717522014393,329.086862218027));
#22279=CARTESIAN_POINT('Ctrl Pts',(150.122790297836,0.364223092970947,329.092368458966));
#22280=CARTESIAN_POINT('Ctrl Pts',(150.130199291221,0.521405380107819,329.104168522329));
#22281=CARTESIAN_POINT('Ctrl Pts',(150.137608284606,0.677728562820399,329.122193048625));
#22282=CARTESIAN_POINT('Ctrl Pts',(150.145021842186,0.834148046005747,329.14022867865));
#22283=CARTESIAN_POINT('Ctrl Pts',(150.152435399766,0.989707002300638,329.164496354932));
#22284=CARTESIAN_POINT('Ctrl Pts',(150.159848957346,1.14387989619223,329.194875596028));
#22285=CARTESIAN_POINT('Ctrl Pts',(150.167273069483,1.29827228342318,329.225298087536));
#22286=CARTESIAN_POINT('Ctrl Pts',(150.17469718162,1.45127430513113,329.261849434873));
#22287=CARTESIAN_POINT('Ctrl Pts',(150.182121293757,1.60237487779323,329.304359095456));
#22288=CARTESIAN_POINT('Ctrl Pts',(150.185978418911,1.68087770870112,329.326444575596));
#22289=CARTESIAN_POINT('Ctrl Pts',(150.189835544066,1.75886760367768,329.350137533726));
#22290=CARTESIAN_POINT('Ctrl Pts',(150.193692669221,1.83627514021165,329.375408977362));
#22291=CARTESIAN_POINT('Ctrl Pts',(150.201116646659,1.98526481042163,329.424050029921));
#22292=CARTESIAN_POINT('Ctrl Pts',(150.208540624097,2.13254522652256,329.478688424302));
#22293=CARTESIAN_POINT('Ctrl Pts',(150.215964601535,2.27759713087014,329.539186702335));
#22294=CARTESIAN_POINT('Ctrl Pts',(150.223379817562,2.42247785214635,329.599613583298));
#22295=CARTESIAN_POINT('Ctrl Pts',(150.23079503359,2.56513495558217,329.665886440144));
#22296=CARTESIAN_POINT('Ctrl Pts',(150.238210249618,2.70506388519565,329.737817948844));
#22297=CARTESIAN_POINT('Ctrl Pts',(150.245618330762,2.84485817589713,329.809680245408));
#22298=CARTESIAN_POINT('Ctrl Pts',(150.253026411906,2.98192918902718,329.887190184902));
#22299=CARTESIAN_POINT('Ctrl Pts',(150.26043449305,3.11579202739832,329.970112267207));
#22300=CARTESIAN_POINT('Ctrl Pts',(150.267837060224,3.24955522921416,330.052972629091));
#22301=CARTESIAN_POINT('Ctrl Pts',(150.275239627398,3.38011469502222,330.141236917048));
#22302=CARTESIAN_POINT('Ctrl Pts',(150.282642194572,3.50700994476609,330.234623644473));
#22303=CARTESIAN_POINT('Ctrl Pts',(150.290040864327,3.63383838471556,330.327961204195));
#22304=CARTESIAN_POINT('Ctrl Pts',(150.297439534081,3.75700615087568,330.426415611613));
#22305=CARTESIAN_POINT('Ctrl Pts',(150.304838203836,3.87608168935596,330.529662059761));
#22306=CARTESIAN_POINT('Ctrl Pts',(150.31223565304,3.9951375840701,330.632891475452));
#22307=CARTESIAN_POINT('Ctrl Pts',(150.319633102244,4.11010230923926,330.740911118658));
#22308=CARTESIAN_POINT('Ctrl Pts',(150.327030551448,4.22057727975467,330.85335581607));
#22309=CARTESIAN_POINT('Ctrl Pts',(150.334427679911,4.33104746026778,330.965795638076));
#22310=CARTESIAN_POINT('Ctrl Pts',(150.341824808375,4.43702801163296,331.082659866581));
#22311=CARTESIAN_POINT('Ctrl Pts',(150.349221936838,4.53815732833411,331.203546572683));
#22312=CARTESIAN_POINT('Ctrl Pts',(150.356620204275,4.63930221642586,331.32445189232));
#22313=CARTESIAN_POINT('Ctrl Pts',(150.364018471712,4.73559414305612,331.449380636512));
#22314=CARTESIAN_POINT('Ctrl Pts',(150.371416739148,4.8267120055567,331.577898046826));
#22315=CARTESIAN_POINT('Ctrl Pts',(150.378817605674,4.91786187872068,331.706460606658));
#22316=CARTESIAN_POINT('Ctrl Pts',(150.3862184722,5.00383385299093,331.838614038472));
#22317=CARTESIAN_POINT('Ctrl Pts',(150.393619338726,5.0843504247341,331.973895024787));
#22318=CARTESIAN_POINT('Ctrl Pts',(150.40102833211,5.16495541137057,332.109324562559));
#22319=CARTESIAN_POINT('Ctrl Pts',(150.408437325495,5.24009284103292,332.247888192523));
#22320=CARTESIAN_POINT('Ctrl Pts',(150.41584631888,5.3095310763227,332.3890977973));
#22321=CARTESIAN_POINT('Ctrl Pts',(150.42325987646,5.37901208796064,332.530394392065));
#22322=CARTESIAN_POINT('Ctrl Pts',(150.43067343404,5.4427867584689,332.674339869234));
#22323=CARTESIAN_POINT('Ctrl Pts',(150.438086991621,5.50067200584216,332.820427095359));
#22324=CARTESIAN_POINT('Ctrl Pts',(150.445511103757,5.55863966346232,332.966722303396));
#22325=CARTESIAN_POINT('Ctrl Pts',(150.452935215894,5.61070102889794,333.115164998965));
#22326=CARTESIAN_POINT('Ctrl Pts',(150.460359328031,5.65672293842651,333.265233110652));
#22327=CARTESIAN_POINT('Ctrl Pts',(150.464216453185,5.68063317329919,333.343199536514));
#22328=CARTESIAN_POINT('Ctrl Pts',(150.46807357834,5.70291406657114,333.421604522187));
#22329=CARTESIAN_POINT('Ctrl Pts',(150.471930703495,5.72355243013718,333.500373999302));
#22330=CARTESIAN_POINT('Ctrl Pts',(150.479354680933,5.76327599090508,333.651985056099));
#22331=CARTESIAN_POINT('Ctrl Pts',(150.486778658371,5.79703128351163,333.805404270438));
#22332=CARTESIAN_POINT('Ctrl Pts',(150.494202635809,5.82465289935838,333.960120600985));
#22333=CARTESIAN_POINT('Ctrl Pts',(150.501617851836,5.85224191754258,334.114654342983));
#22334=CARTESIAN_POINT('Ctrl Pts',(150.509033067864,5.8737116026831,334.270481790294));
#22335=CARTESIAN_POINT('Ctrl Pts',(150.516448283892,5.88894643536034,334.427077279245));
#22336=CARTESIAN_POINT('Ctrl Pts',(150.523856365036,5.90416660915828,334.583522092806));
#22337=CARTESIAN_POINT('Ctrl Pts',(150.53126444618,5.91316383777285,334.740733107809));
#22338=CARTESIAN_POINT('Ctrl Pts',(150.538672527324,5.91587375258846,334.898175121238));
#22339=CARTESIAN_POINT('Ctrl Pts',(150.546075094498,5.91858165036497,335.0554999477));
#22340=CARTESIAN_POINT('Ctrl Pts',(150.553477661672,5.91501154603593,335.213055058679));
#22341=CARTESIAN_POINT('Ctrl Pts',(150.560880228846,5.90515095550929,335.370300898119));
#22342=CARTESIAN_POINT('Ctrl Pts',(150.568278898601,5.89529555654051,335.527463948312));
#22343=CARTESIAN_POINT('Ctrl Pts',(150.575677568355,5.87915629054507,335.68431767971));
#22344=CARTESIAN_POINT('Ctrl Pts',(150.58307623811,5.85677275605526,335.840323417756));
#22345=CARTESIAN_POINT('Ctrl Pts',(150.590473687314,5.83439291415345,335.9963034197));
#22346=CARTESIAN_POINT('Ctrl Pts',(150.597871136518,5.80577090114714,336.151435336864));
#22347=CARTESIAN_POINT('Ctrl Pts',(150.605268585722,5.77099810178896,336.305186374296));
#22348=CARTESIAN_POINT('Ctrl Pts',(150.612665714185,5.73622681011875,336.458930745351));
#22349=CARTESIAN_POINT('Ctrl Pts',(150.620062842649,5.69530534468638,336.611293991702));
#22350=CARTESIAN_POINT('Ctrl Pts',(150.627459971112,5.64837601058656,336.761754524765));
#22351=CARTESIAN_POINT('Ctrl Pts',(150.634858238549,5.6014394505408,336.912238224994));
#22352=CARTESIAN_POINT('Ctrl Pts',(150.642256505986,5.54849329104085,337.060818272288));
#22353=CARTESIAN_POINT('Ctrl Pts',(150.649654773422,5.48972936265013,337.206989371827));
#22354=CARTESIAN_POINT('Ctrl Pts',(150.657055639948,5.43094478987323,337.353211822811));
#22355=CARTESIAN_POINT('Ctrl Pts',(150.664456506474,5.36633851803954,337.497023295023));
#22356=CARTESIAN_POINT('Ctrl Pts',(150.671857373,5.29614998756381,337.637939702064));
#22357=CARTESIAN_POINT('Ctrl Pts',(150.679266366384,5.22588438337137,337.779010848793));
#22358=CARTESIAN_POINT('Ctrl Pts',(150.686675359769,5.1500244453845,337.917180247335));
#22359=CARTESIAN_POINT('Ctrl Pts',(150.694084353154,5.0688552896325,338.051988960541));
#22360=CARTESIAN_POINT('Ctrl Pts',(150.701497910734,4.98763613088067,338.186880720564));
#22361=CARTESIAN_POINT('Ctrl Pts',(150.708911468314,4.90110144178917,338.318407358853));
#22362=CARTESIAN_POINT('Ctrl Pts',(150.716325025895,4.8095786055142,338.446140478837));
#22363=CARTESIAN_POINT('Ctrl Pts',(150.723749138031,4.7179254697265,338.574055450302));
#22364=CARTESIAN_POINT('Ctrl Pts',(150.731173250168,4.62127023225375,338.69816582339));
#22365=CARTESIAN_POINT('Ctrl Pts',(150.738597362305,4.51997985155643,338.818077095086));
#22366=CARTESIAN_POINT('Ctrl Pts',(150.742454487459,4.46735542076684,338.88037582844));
#22367=CARTESIAN_POINT('Ctrl Pts',(150.746311612614,4.41348046544508,338.941541743558));
#22368=CARTESIAN_POINT('Ctrl Pts',(150.750168737769,4.35841013442152,339.001523667639));
#22369=CARTESIAN_POINT('Ctrl Pts',(150.757592715207,4.25241386034981,339.116973499627));
#22370=CARTESIAN_POINT('Ctrl Pts',(150.765016692645,4.14166729566465,339.228382985388));
#22371=CARTESIAN_POINT('Ctrl Pts',(150.772440670083,4.02651067384282,339.335336475515));
#22372=CARTESIAN_POINT('Ctrl Pts',(150.77985588611,3.91148995416092,339.442163744431));
#22373=CARTESIAN_POINT('Ctrl Pts',(150.787271102138,3.79206980784507,339.544545233818));
#22374=CARTESIAN_POINT('Ctrl Pts',(150.794686318166,3.66862976250432,339.642099334156));
#22375=CARTESIAN_POINT('Ctrl Pts',(150.80209439931,3.5453084905537,339.739559568429));
#22376=CARTESIAN_POINT('Ctrl Pts',(150.809502480454,3.41797531075208,339.832201430903));
#22377=CARTESIAN_POINT('Ctrl Pts',(150.816910561598,3.28704545318422,339.919681163572));
#22378=CARTESIAN_POINT('Ctrl Pts',(150.824313128772,3.15621304910097,340.007095783477));
#22379=CARTESIAN_POINT('Ctrl Pts',(150.831715695946,3.02178960668352,340.089355717643));
#22380=CARTESIAN_POINT('Ctrl Pts',(150.83911826312,2.88422209427119,340.166158483188));
#22381=CARTESIAN_POINT('Ctrl Pts',(150.846516932874,2.74672701055279,340.242920812413));
#22382=CARTESIAN_POINT('Ctrl Pts',(150.853915602629,2.60609147859102,340.314231513647));
#22383=CARTESIAN_POINT('Ctrl Pts',(150.861314272384,2.46278991035233,340.379832378427));
#22384=CARTESIAN_POINT('Ctrl Pts',(150.868711721588,2.31951198242234,340.445422421101));
#22385=CARTESIAN_POINT('Ctrl Pts',(150.876109170792,2.17356923011666,340.505304341585));
#22386=CARTESIAN_POINT('Ctrl Pts',(150.883506619996,2.02545914561065,340.559266661347));
#22387=CARTESIAN_POINT('Ctrl Pts',(150.890903748459,1.87735548289982,340.613226641396));
#22388=CARTESIAN_POINT('Ctrl Pts',(150.898300876923,1.72708502549775,340.661267403295));
#22389=CARTESIAN_POINT('Ctrl Pts',(150.905698005386,1.57516339782496,340.703226352921));
#22390=CARTESIAN_POINT('Ctrl Pts',(150.913096272823,1.42321837801344,340.745191763178));
#22391=CARTESIAN_POINT('Ctrl Pts',(150.920494540259,1.26962204147258,340.78107339721));
#22392=CARTESIAN_POINT('Ctrl Pts',(150.927892807696,1.11490311192077,340.810759125409));
#22393=CARTESIAN_POINT('Ctrl Pts',(150.935293674222,0.960129827981612,340.840455282518));
#22394=CARTESIAN_POINT('Ctrl Pts',(150.942694540747,0.804233532118901,340.863951129733));
#22395=CARTESIAN_POINT('Ctrl Pts',(150.950095407273,0.647750877860981,340.881186050681));
#22396=CARTESIAN_POINT('Ctrl Pts',(150.957504400658,0.491096390688802,340.898439897221));
#22397=CARTESIAN_POINT('Ctrl Pts',(150.964913394043,0.333854630452807,340.909419046677));
#22398=CARTESIAN_POINT('Ctrl Pts',(150.972322387427,0.176565819838281,340.914114901975));
#22399=CARTESIAN_POINT('Ctrl Pts',(150.979735945008,0.0191801138904138,
340.918813650082));
#22400=CARTESIAN_POINT('Ctrl Pts',(150.987149502588,-0.138252327871474,
340.917221394864));
#22401=CARTESIAN_POINT('Ctrl Pts',(150.994563060168,-0.295194091819947,
340.909381609835));
#22402=CARTESIAN_POINT('Ctrl Pts',(151.001987172305,-0.452359291100679,
340.901530663436));
#22403=CARTESIAN_POINT('Ctrl Pts',(151.009411284441,-0.609032046681527,
340.887414456526));
#22404=CARTESIAN_POINT('Ctrl Pts',(151.016835396578,-0.76468203028186,340.867128084085));
#22405=CARTESIAN_POINT('Ctrl Pts',(151.020692521733,-0.845548463337213,
340.856588496859));
#22406=CARTESIAN_POINT('Ctrl Pts',(151.024549646888,-0.926139015950719,
340.844384283927));
#22407=CARTESIAN_POINT('Ctrl Pts',(151.028406772043,-1.00638081162408,340.830534128576));
#22408=CARTESIAN_POINT('Ctrl Pts',(151.035830749481,-1.16082570432244,340.803876128977));
#22409=CARTESIAN_POINT('Ctrl Pts',(151.043254726919,-1.3144436385046,340.771037045479));
#22410=CARTESIAN_POINT('Ctrl Pts',(151.050678704357,-1.46670096585834,340.732078055928));
#22411=CARTESIAN_POINT('Ctrl Pts',(151.058093920384,-1.61877860665737,340.693165043846));
#22412=CARTESIAN_POINT('Ctrl Pts',(151.065509136412,-1.76949847879413,340.648146593647));
#22413=CARTESIAN_POINT('Ctrl Pts',(151.072924352439,-1.91833429451591,340.597135347388));
#22414=CARTESIAN_POINT('Ctrl Pts',(151.080332433584,-2.06702690116564,340.546173183893));
#22415=CARTESIAN_POINT('Ctrl Pts',(151.087740514728,-2.21383870971484,340.489229824037));
#22416=CARTESIAN_POINT('Ctrl Pts',(151.095148595872,-2.35825594189839,340.426468416475));
#22417=CARTESIAN_POINT('Ctrl Pts',(151.102551163046,-2.50256568169828,340.363753723375));
#22418=CARTESIAN_POINT('Ctrl Pts',(151.10995373022,-2.64448405318538,340.295229753298));
#22419=CARTESIAN_POINT('Ctrl Pts',(151.117356297394,-2.78351481183673,340.221108680614));
#22420=CARTESIAN_POINT('Ctrl Pts',(151.124754967149,-2.92247237140334,340.14702663235));
#22421=CARTESIAN_POINT('Ctrl Pts',(151.132153636904,-3.05854501742987,340.067353525439));
#22422=CARTESIAN_POINT('Ctrl Pts',(151.139552306658,-3.19125888537502,339.982348571609));
#22423=CARTESIAN_POINT('Ctrl Pts',(151.146949755862,-3.32395085965103,339.897357640959));
#22424=CARTESIAN_POINT('Ctrl Pts',(151.154347205066,-3.4532848415771,339.80703681019));
#22425=CARTESIAN_POINT('Ctrl Pts',(151.16174465427,-3.57881377278148,339.711689987918));
#22426=CARTESIAN_POINT('Ctrl Pts',(151.169141782734,-3.70433726127045,339.616347299719));
#22427=CARTESIAN_POINT('Ctrl Pts',(151.176538911197,-3.82605572987341,339.51597927905));
#22428=CARTESIAN_POINT('Ctrl Pts',(151.183936039661,-3.94355341576413,339.41093153648));
#22429=CARTESIAN_POINT('Ctrl Pts',(151.191334307098,-4.06106919336495,339.30586761918));
#22430=CARTESIAN_POINT('Ctrl Pts',(151.198732574534,-4.17436261598112,339.196122794011));
#22431=CARTESIAN_POINT('Ctrl Pts',(151.206130841971,-4.28305326869173,339.082080996263));
#22432=CARTESIAN_POINT('Ctrl Pts',(151.213531708496,-4.39178210557177,338.967999134431));
#22433=CARTESIAN_POINT('Ctrl Pts',(151.220932575022,-4.49590469577555,338.849617564458));
#22434=CARTESIAN_POINT('Ctrl Pts',(151.228333441548,-4.59507965168306,338.727354766747));
#22435=CARTESIAN_POINT('Ctrl Pts',(151.235742434933,-4.69436351117357,338.604957712794));
#22436=CARTESIAN_POINT('Ctrl Pts',(151.243151428318,-4.78868865117479,338.47867120976));
#22437=CARTESIAN_POINT('Ctrl Pts',(151.250560421702,-4.87775549673004,338.348944890054));
#22438=CARTESIAN_POINT('Ctrl Pts',(151.257973979282,-4.9668772105343,338.219138654461));
#22439=CARTESIAN_POINT('Ctrl Pts',(151.265387536863,-5.05073397686028,338.085888694848));
#22440=CARTESIAN_POINT('Ctrl Pts',(151.272801094443,-5.12907152816297,337.949670459812));
#22441=CARTESIAN_POINT('Ctrl Pts',(151.28022520658,-5.20752060731175,337.81325829318));
#22442=CARTESIAN_POINT('Ctrl Pts',(151.287649318716,-5.28043460569062,337.673869740998));
#22443=CARTESIAN_POINT('Ctrl Pts',(151.295073430853,-5.34760649963432,337.532002228982));
#22444=CARTESIAN_POINT('Ctrl Pts',(151.298930556008,-5.38250500292219,337.458296344811));
#22445=CARTESIAN_POINT('Ctrl Pts',(151.302787681162,-5.41585439220377,337.383921629904));
#22446=CARTESIAN_POINT('Ctrl Pts',(151.306644806317,-5.44763094099968,337.308949478261));
#22447=CARTESIAN_POINT('Ctrl Pts',(151.314899635015,-5.51563754084358,337.148497783242));
#22448=CARTESIAN_POINT('Ctrl Pts',(151.323154463714,-5.57661208907137,336.984896632829));
#22449=CARTESIAN_POINT('Ctrl Pts',(151.331409292412,-5.63028344227576,336.818746524982));
#22450=CARTESIAN_POINT('Ctrl Pts',(151.339630362242,-5.68373530162608,336.653275903032));
#22451=CARTESIAN_POINT('Ctrl Pts',(151.347851432071,-5.72994346593964,336.485277332685));
#22452=CARTESIAN_POINT('Ctrl Pts',(151.356072501901,-5.76868604797543,336.31536756931));
#22453=CARTESIAN_POINT('Ctrl Pts',(151.364271623208,-5.80732519548824,336.145911429169));
#22454=CARTESIAN_POINT('Ctrl Pts',(151.372470744515,-5.83853845578075,335.974554492344));
#22455=CARTESIAN_POINT('Ctrl Pts',(151.380669865822,-5.86215321702131,335.801929063363));
#22456=CARTESIAN_POINT('Ctrl Pts',(151.388833272724,-5.8856651151465,335.630055570395));
#22457=CARTESIAN_POINT('Ctrl Pts',(151.396996679625,-5.90164447442005,335.456924828824));
#22458=CARTESIAN_POINT('Ctrl Pts',(151.405160086527,-5.90996960527333,335.283178083978));
#22459=CARTESIAN_POINT('Ctrl Pts',(151.409540577134,-5.91443687708099,335.189945443122));
#22460=CARTESIAN_POINT('Ctrl Pts',(151.413921067741,-5.91670102869276,335.096535704654));
#22461=CARTESIAN_POINT('Ctrl Pts',(151.418301558348,-5.91674921405907,335.003049660855));
#22462=CARTESIAN_POINT('',(153.168301655484,-5.91514362196022,334.995017318901));
#22463=CARTESIAN_POINT('Ctrl Pts',(151.418301620294,-5.90851180222765,335.003044094879));
#22464=CARTESIAN_POINT('Ctrl Pts',(151.473828693726,-5.90301154998691,333.819662210617));
#22465=CARTESIAN_POINT('Ctrl Pts',(151.622101778582,-4.98404225688584,330.651831516879));
#22466=CARTESIAN_POINT('Ctrl Pts',(151.863120874865,0.183842817904274,328.005800636274));
#22467=CARTESIAN_POINT('Ctrl Pts',(152.141358909138,5.98105935732207,331.369634744905));
#22468=CARTESIAN_POINT('Ctrl Pts',(152.419596943413,6.2895460048169,338.06500146403));
#22469=CARTESIAN_POINT('Ctrl Pts',(152.697834977687,0.826209117236143,341.947661578966));
#22470=CARTESIAN_POINT('Ctrl Pts',(152.947403203314,-4.75425691722228,339.711446338383));
#22471=CARTESIAN_POINT('Ctrl Pts',(153.104225417516,-5.90156738596128,336.358344737351));
#22472=CARTESIAN_POINT('Ctrl Pts',(153.168301620294,-5.91239802015065,334.995020380605));
#22473=CARTESIAN_POINT('',(154.918301620294,-5.92100069945767,334.999282630589));
#22474=CARTESIAN_POINT('Ctrl Pts',(153.168301676046,-5.91674790045664,334.995015529921));
#22475=CARTESIAN_POINT('Ctrl Pts',(153.177127639827,-5.91658958741957,334.807092177029));
#22476=CARTESIAN_POINT('Ctrl Pts',(153.185953603608,-5.90747449529418,334.6195553215));
#22477=CARTESIAN_POINT('Ctrl Pts',(153.194779567389,-5.88953568797227,334.433166741801));
#22478=CARTESIAN_POINT('Ctrl Pts',(153.203671549467,-5.87146269819447,334.245383973685));
#22479=CARTESIAN_POINT('Ctrl Pts',(153.212563531544,-5.84443359370318,334.058766748309));
#22480=CARTESIAN_POINT('Ctrl Pts',(153.221455513621,-5.80863311473178,333.874072870501));
#22481=CARTESIAN_POINT('Ctrl Pts',(153.230419364663,-5.77254328032391,333.687886214407));
#22482=CARTESIAN_POINT('Ctrl Pts',(153.239383215705,-5.72753976335944,333.503654142379));
#22483=CARTESIAN_POINT('Ctrl Pts',(153.248347066747,-5.67385995749029,333.322131189488));
#22484=CARTESIAN_POINT('Ctrl Pts',(153.250335059909,-5.66195490836465,333.281873225872));
#22485=CARTESIAN_POINT('Ctrl Pts',(153.252323053071,-5.64962329295002,333.241748427726));
#22486=CARTESIAN_POINT('Ctrl Pts',(153.254311046233,-5.63686801497755,333.201764880717));
#22487=CARTESIAN_POINT('Ctrl Pts',(153.261735023671,-5.58923460371215,333.052450005522));
#22488=CARTESIAN_POINT('Ctrl Pts',(153.269159001109,-5.53559244025597,332.904803829118));
#22489=CARTESIAN_POINT('Ctrl Pts',(153.276582978547,-5.47607547168731,332.759346525925));
#22490=CARTESIAN_POINT('Ctrl Pts',(153.283998194575,-5.41662874209636,332.614060884235));
#22491=CARTESIAN_POINT('Ctrl Pts',(153.291413410602,-5.35132114790566,332.470959315914));
#22492=CARTESIAN_POINT('Ctrl Pts',(153.29882862663,-5.2803366002361,332.330547630935));
#22493=CARTESIAN_POINT('Ctrl Pts',(153.306236707774,-5.20942035354087,332.190271049372));
#22494=CARTESIAN_POINT('Ctrl Pts',(153.313644788918,-5.13283819511548,332.052679529387));
#22495=CARTESIAN_POINT('Ctrl Pts',(153.321052870062,-5.05082234388107,331.918259548072));
#22496=CARTESIAN_POINT('Ctrl Pts',(153.328455437236,-4.96886753854256,331.783939618003));
#22497=CARTESIAN_POINT('Ctrl Pts',(153.33585800441,-4.88148728693261,331.652786843465));
#22498=CARTESIAN_POINT('Ctrl Pts',(153.343260571584,-4.78895995835898,331.525263595647));
#22499=CARTESIAN_POINT('Ctrl Pts',(153.350659241339,-4.69648134501969,331.397807488263));
#22500=CARTESIAN_POINT('Ctrl Pts',(153.358057911093,-4.59886127029452,331.273977403181));
#22501=CARTESIAN_POINT('Ctrl Pts',(153.365456580848,-4.49642161828097,331.154207078748));
#22502=CARTESIAN_POINT('Ctrl Pts',(153.372854030052,-4.39399886562891,331.034456512698));
#22503=CARTESIAN_POINT('Ctrl Pts',(153.380251479256,-4.28675835601205,330.918764661436));
#22504=CARTESIAN_POINT('Ctrl Pts',(153.38764892846,-4.17506256167947,330.807532567978));
#22505=CARTESIAN_POINT('Ctrl Pts',(153.395046056924,-4.06337161028184,330.696305297351));
#22506=CARTESIAN_POINT('Ctrl Pts',(153.402443185387,-3.9472260227094,330.589537663401));
#22507=CARTESIAN_POINT('Ctrl Pts',(153.409840313851,-3.82702527578928,330.48759397871));
#22508=CARTESIAN_POINT('Ctrl Pts',(153.417238581287,-3.70680602095469,330.385634597237));
#22509=CARTESIAN_POINT('Ctrl Pts',(153.424636848724,-3.58253064816983,330.288500885382));
#22510=CARTESIAN_POINT('Ctrl Pts',(153.432035116161,-3.45463173667,330.19651687559));
#22511=CARTESIAN_POINT('Ctrl Pts',(153.439435982686,-3.32668789293758,330.104500550848));
#22512=CARTESIAN_POINT('Ctrl Pts',(153.446836849212,-3.19511827877351,330.017637747942));
#22513=CARTESIAN_POINT('Ctrl Pts',(153.454237715738,-3.06038432635086,329.936209094213));
#22514=CARTESIAN_POINT('Ctrl Pts',(153.461646709123,-2.92550242316721,329.854691024038));
#22515=CARTESIAN_POINT('Ctrl Pts',(153.469055702508,-2.7874495620714,329.778619213042));
#22516=CARTESIAN_POINT('Ctrl Pts',(153.476464695892,-2.64671228442733,329.70822859092));
#22517=CARTESIAN_POINT('Ctrl Pts',(153.483878253473,-2.50588830776578,329.637794605745));
#22518=CARTESIAN_POINT('Ctrl Pts',(153.491291811053,-2.36237695875122,329.573048936395));
#22519=CARTESIAN_POINT('Ctrl Pts',(153.498705368633,-2.21668412240818,329.514178086744));
#22520=CARTESIAN_POINT('Ctrl Pts',(153.50612948077,-2.07078386564008,329.45522342366));
#22521=CARTESIAN_POINT('Ctrl Pts',(153.513553592907,-1.92269626913605,329.402160410171));
#22522=CARTESIAN_POINT('Ctrl Pts',(153.520977705043,-1.77294249278271,329.355125733926));
#22523=CARTESIAN_POINT('Ctrl Pts',(153.524834830198,-1.69513937677696,329.330689325968));
#22524=CARTESIAN_POINT('Ctrl Pts',(153.528691955353,-1.61688670360662,329.307879259645));
#22525=CARTESIAN_POINT('Ctrl Pts',(153.532549080508,-1.5382584508544,329.286709223147));
#22526=CARTESIAN_POINT('Ctrl Pts',(153.539973057946,-1.38691921476956,329.245962328241));
#22527=CARTESIAN_POINT('Ctrl Pts',(153.547397035384,-1.23373154250453,329.211171349908));
#22528=CARTESIAN_POINT('Ctrl Pts',(153.554821012822,-1.07920534627867,329.18250514542));
#22529=CARTESIAN_POINT('Ctrl Pts',(153.56223622885,-0.924861514214024,329.153872771367));
#22530=CARTESIAN_POINT('Ctrl Pts',(153.569651444877,-0.769182665908337,
329.131350850813));
#22531=CARTESIAN_POINT('Ctrl Pts',(153.577066660905,-0.612693672621006,
329.115058451775));
#22532=CARTESIAN_POINT('Ctrl Pts',(153.584474742049,-0.45635525225506,329.0987817292));
#22533=CARTESIAN_POINT('Ctrl Pts',(153.591882823193,-0.299208607505325,
329.088722633565));
#22534=CARTESIAN_POINT('Ctrl Pts',(153.599290904337,-0.14178849432088,329.084949147693));
#22535=CARTESIAN_POINT('Ctrl Pts',(153.606693471511,0.0155144481982303,
329.081178470495));
#22536=CARTESIAN_POINT('Ctrl Pts',(153.614096038685,0.173090082353266,329.083684096403));
#22537=CARTESIAN_POINT('Ctrl Pts',(153.621498605859,0.33039894874051,329.092482154308));
#22538=CARTESIAN_POINT('Ctrl Pts',(153.628897275614,0.487624992697058,329.101275580074));
#22539=CARTESIAN_POINT('Ctrl Pts',(153.636295945369,0.644584176913965,329.116354819137));
#22540=CARTESIAN_POINT('Ctrl Pts',(153.643694615124,0.80073757160893,329.137683912999));
#22541=CARTESIAN_POINT('Ctrl Pts',(153.651092064327,0.956865205842703,329.159009488222));
#22542=CARTESIAN_POINT('Ctrl Pts',(153.658489513531,1.11218694495993,329.18658282152));
#22543=CARTESIAN_POINT('Ctrl Pts',(153.665886962735,1.26616938879767,329.220316129634));
#22544=CARTESIAN_POINT('Ctrl Pts',(153.673284091199,1.42014515622504,329.25404797513));
#22545=CARTESIAN_POINT('Ctrl Pts',(153.680681219662,1.57278137926868,329.293939184522));
#22546=CARTESIAN_POINT('Ctrl Pts',(153.688078348126,1.72355551987454,329.339850979664));
#22547=CARTESIAN_POINT('Ctrl Pts',(153.695476615562,1.87435287593434,329.385769844077));
#22548=CARTESIAN_POINT('Ctrl Pts',(153.702874882999,2.02328722162326,329.437711031335));
#22549=CARTESIAN_POINT('Ctrl Pts',(153.710273150435,2.16985197770115,329.495486128879));
#22550=CARTESIAN_POINT('Ctrl Pts',(153.717674016961,2.31646822351918,329.553281523422));
#22551=CARTESIAN_POINT('Ctrl Pts',(153.725074883487,2.46071287530637,329.616914772049));
#22552=CARTESIAN_POINT('Ctrl Pts',(153.732475750013,2.60210024011964,329.686149710157));
#22553=CARTESIAN_POINT('Ctrl Pts',(153.739884743397,2.74364286177669,329.755460674845));
#22554=CARTESIAN_POINT('Ctrl Pts',(153.747293736782,2.88232159517437,329.83038544904));
#22555=CARTESIAN_POINT('Ctrl Pts',(153.754702730167,3.01767558747218,329.910642023666));
#22556=CARTESIAN_POINT('Ctrl Pts',(153.762116287747,3.15311296249817,329.99094803911));
#22557=CARTESIAN_POINT('Ctrl Pts',(153.769529845327,3.28522120277456,330.076592197386));
#22558=CARTESIAN_POINT('Ctrl Pts',(153.776943402907,3.41356970979961,330.167250016933));
#22559=CARTESIAN_POINT('Ctrl Pts',(153.784367515044,3.54210094442163,330.258036904482));
#22560=CARTESIAN_POINT('Ctrl Pts',(153.791791627181,3.66686146024687,330.35385148234));
#22561=CARTESIAN_POINT('Ctrl Pts',(153.799215739317,3.78745428419734,330.454329465567));
#22562=CARTESIAN_POINT('Ctrl Pts',(153.803072864472,3.85010711138703,330.506531823164));
#22563=CARTESIAN_POINT('Ctrl Pts',(153.806929989627,3.91163559437647,330.55999232975));
#22564=CARTESIAN_POINT('Ctrl Pts',(153.810787114781,3.97198818896083,330.614656183461));
#22565=CARTESIAN_POINT('Ctrl Pts',(153.818211092219,4.08815146667361,330.719870092876));
#22566=CARTESIAN_POINT('Ctrl Pts',(153.825635069657,4.20030658195626,330.829861479918));
#22567=CARTESIAN_POINT('Ctrl Pts',(153.833059047095,4.30803559636577,330.944292926881));
#22568=CARTESIAN_POINT('Ctrl Pts',(153.840474263123,4.41563747432958,331.05858932752));
#22569=CARTESIAN_POINT('Ctrl Pts',(153.847889479151,4.51882339547609,331.177315088804));
#22570=CARTESIAN_POINT('Ctrl Pts',(153.855304695178,4.61720919501505,331.300093269828));
#22571=CARTESIAN_POINT('Ctrl Pts',(153.862712776322,4.71550032823311,331.422753314305));
#22572=CARTESIAN_POINT('Ctrl Pts',(153.870120857467,4.8090003029009,331.549457726613));
#22573=CARTESIAN_POINT('Ctrl Pts',(153.877528938611,4.89736256368294,331.679793608473));
#22574=CARTESIAN_POINT('Ctrl Pts',(153.884931505785,4.98565905482044,331.810032478956));
#22575=CARTESIAN_POINT('Ctrl Pts',(153.892334072959,5.06882523786897,331.943897129397));
#22576=CARTESIAN_POINT('Ctrl Pts',(153.899736640133,5.14655561726123,332.080942645144));
#22577=CARTESIAN_POINT('Ctrl Pts',(153.907135309888,5.22424507194852,332.217916007027));
#22578=CARTESIAN_POINT('Ctrl Pts',(153.914533979642,5.29650423901483,332.358066575116));
#22579=CARTESIAN_POINT('Ctrl Pts',(153.921932649397,5.36307171089967,332.500921692654));
#22580=CARTESIAN_POINT('Ctrl Pts',(153.929330098601,5.42962820121868,332.643753243533));
#22581=CARTESIAN_POINT('Ctrl Pts',(153.936727547805,5.49049470239322,332.789288120406));
#22582=CARTESIAN_POINT('Ctrl Pts',(153.944124997009,5.54545637980306,332.937030271138));
#22583=CARTESIAN_POINT('Ctrl Pts',(153.951522125473,5.60041567417038,333.084766016028));
#22584=CARTESIAN_POINT('Ctrl Pts',(153.958919253936,5.6494705237047,333.234708494695));
#22585=CARTESIAN_POINT('Ctrl Pts',(153.9663163824,5.69245485458461,333.386343192926));
#22586=CARTESIAN_POINT('Ctrl Pts',(153.973714649836,5.73544580397847,333.538001239115));
#22587=CARTESIAN_POINT('Ctrl Pts',(153.981112917273,5.77236427179964,333.69135166459));
#22588=CARTESIAN_POINT('Ctrl Pts',(153.988511184709,5.80309455909471,333.845866515214));
#22589=CARTESIAN_POINT('Ctrl Pts',(153.995912051235,5.83383564226289,334.000435648529));
#22590=CARTESIAN_POINT('Ctrl Pts',(154.003312917761,5.85838414377514,334.156169655649));
#22591=CARTESIAN_POINT('Ctrl Pts',(154.010713784287,5.8766758231634,334.312532304798));
#22592=CARTESIAN_POINT('Ctrl Pts',(154.018122777672,5.89498758856439,334.469066655084));
#22593=CARTESIAN_POINT('Ctrl Pts',(154.025531771056,5.90702876751917,334.626230655079));
#22594=CARTESIAN_POINT('Ctrl Pts',(154.032940764441,5.91278711356018,334.783484152505));
#22595=CARTESIAN_POINT('Ctrl Pts',(154.040354322021,5.91854900694098,334.940834523509));
#22596=CARTESIAN_POINT('Ctrl Pts',(154.047767879602,5.91802035629129,335.098274129467));
#22597=CARTESIAN_POINT('Ctrl Pts',(154.055181437182,5.91124100352163,335.255265275321));
#22598=CARTESIAN_POINT('Ctrl Pts',(154.062605549319,5.90445199910218,335.412479926812));
#22599=CARTESIAN_POINT('Ctrl Pts',(154.070029661455,5.89139455033729,335.569244472136));
#22600=CARTESIAN_POINT('Ctrl Pts',(154.077453773592,5.87216016729201,335.725027952681));
#22601=CARTESIAN_POINT('Ctrl Pts',(154.081310898747,5.86216713091127,335.805963742768));
#22602=CARTESIAN_POINT('Ctrl Pts',(154.085168023901,5.85050764304288,335.88663490444));
#22603=CARTESIAN_POINT('Ctrl Pts',(154.089025149056,5.83719989421586,335.966968436644));
#22604=CARTESIAN_POINT('Ctrl Pts',(154.096449126494,5.81158588816656,336.121589898665));
#22605=CARTESIAN_POINT('Ctrl Pts',(154.103873103932,5.7797853525786,336.275426178662));
#22606=CARTESIAN_POINT('Ctrl Pts',(154.11129708137,5.74185585872572,336.427943227204));
#22607=CARTESIAN_POINT('Ctrl Pts',(154.118712297397,5.70397112738237,336.58028028268));
#22608=CARTESIAN_POINT('Ctrl Pts',(154.126127513425,5.65997192455523,336.731300847061));
#22609=CARTESIAN_POINT('Ctrl Pts',(154.133542729453,5.60996733428095,336.880477883624));
#22610=CARTESIAN_POINT('Ctrl Pts',(154.140950810597,5.56001085817168,337.029511382795));
#22611=CARTESIAN_POINT('Ctrl Pts',(154.148358891741,5.50406061606234,337.176704534024));
#22612=CARTESIAN_POINT('Ctrl Pts',(154.155766972885,5.44227628194723,337.321542468587));
#22613=CARTESIAN_POINT('Ctrl Pts',(154.163169540059,5.38053793504038,337.46627259763));
#22614=CARTESIAN_POINT('Ctrl Pts',(154.170572107233,5.31297428832971,337.608650658734));
#22615=CARTESIAN_POINT('Ctrl Pts',(154.177974674407,5.23979415885737,337.748178985311));
#22616=CARTESIAN_POINT('Ctrl Pts',(154.185373344162,5.1666525584033,337.887633850833));
#22617=CARTESIAN_POINT('Ctrl Pts',(154.192772013916,5.08790053724582,338.024241640232));
#22618=CARTESIAN_POINT('Ctrl Pts',(154.200170683671,5.00379409990611,338.157526748619));
#22619=CARTESIAN_POINT('Ctrl Pts',(154.207568132875,4.91970153751694,338.290789869102));
#22620=CARTESIAN_POINT('Ctrl Pts',(154.214965582079,4.83025651100921,338.420731081134));
#22621=CARTESIAN_POINT('Ctrl Pts',(154.222363031283,4.73575990186539,338.546901283428));
#22622=CARTESIAN_POINT('Ctrl Pts',(154.229760159746,4.64126738992983,338.673066015202));
#22623=CARTESIAN_POINT('Ctrl Pts',(154.23715728821,4.54172395458583,338.795459763619));
#22624=CARTESIAN_POINT('Ctrl Pts',(154.244554416673,4.43747238973926,338.913664440496));
#22625=CARTESIAN_POINT('Ctrl Pts',(154.25195268411,4.33320477275411,339.031887317942));
#22626=CARTESIAN_POINT('Ctrl Pts',(154.259350951546,4.22422782970407,339.145919559624));
#22627=CARTESIAN_POINT('Ctrl Pts',(154.266749218983,4.1109229171443,339.255378165545));
#22628=CARTESIAN_POINT('Ctrl Pts',(154.274150085509,3.99757819937722,339.364875225425));
#22629=CARTESIAN_POINT('Ctrl Pts',(154.281550952035,3.87990275311245,339.469795191334));
#22630=CARTESIAN_POINT('Ctrl Pts',(154.28895181856,3.75831274288632,339.569793856309));
#22631=CARTESIAN_POINT('Ctrl Pts',(154.296360811945,3.63658921520443,339.669902329378));
#22632=CARTESIAN_POINT('Ctrl Pts',(154.30376980533,3.5109428275175,339.765078472114));
#22633=CARTESIAN_POINT('Ctrl Pts',(154.311178798714,3.38182117813344,339.85501967881));
#22634=CARTESIAN_POINT('Ctrl Pts',(154.318592356295,3.2526199853595,339.945016292391));
#22635=CARTESIAN_POINT('Ctrl Pts',(154.326005913875,3.11993957868273,340.029771343448));
#22636=CARTESIAN_POINT('Ctrl Pts',(154.333419471455,2.98425367809265,340.109027358244));
#22637=CARTESIAN_POINT('Ctrl Pts',(154.340843583592,2.84837460378246,340.188396208488));
#22638=CARTESIAN_POINT('Ctrl Pts',(154.348267695728,2.70948181843196,340.262250211876));
#22639=CARTESIAN_POINT('Ctrl Pts',(154.355691807865,2.56807133781314,340.330378989003));
#22640=CARTESIAN_POINT('Ctrl Pts',(154.35954893302,2.49460289984933,340.365774631631));
#22641=CARTESIAN_POINT('Ctrl Pts',(154.363406058175,2.42045518104374,340.399625714032));
#22642=CARTESIAN_POINT('Ctrl Pts',(154.36726318333,2.34569941347926,340.43190802795));
#22643=CARTESIAN_POINT('Ctrl Pts',(154.374687160768,2.20181371895697,340.494043209089));
#22644=CARTESIAN_POINT('Ctrl Pts',(154.382111138206,2.05524041463205,340.550551098509));
#22645=CARTESIAN_POINT('Ctrl Pts',(154.389535115644,1.90645974918681,340.60119110433));
#22646=CARTESIAN_POINT('Ctrl Pts',(154.396950331671,1.75785466731193,340.651771347326));
#22647=CARTESIAN_POINT('Ctrl Pts',(154.404365547699,1.60704775951795,340.696497371931));
#22648=CARTESIAN_POINT('Ctrl Pts',(154.411780763727,1.45454125385807,340.735175699429));
#22649=CARTESIAN_POINT('Ctrl Pts',(154.419188844871,1.30218148919004,340.773816810836));
#22650=CARTESIAN_POINT('Ctrl Pts',(154.426596926015,1.1481257416625,340.806421718672));
#22651=CARTESIAN_POINT('Ctrl Pts',(154.434005007159,0.992893384131786,340.832846071194));
#22652=CARTESIAN_POINT('Ctrl Pts',(154.441407574333,0.837776568879942,340.859250755589));
#22653=CARTESIAN_POINT('Ctrl Pts',(154.448810141507,0.681485253758091,340.879483982177));
#22654=CARTESIAN_POINT('Ctrl Pts',(154.456212708681,0.52455094010036,340.893452033718));
#22655=CARTESIAN_POINT('Ctrl Pts',(154.463611378436,0.367699251672922,340.907412731142));
#22656=CARTESIAN_POINT('Ctrl Pts',(154.471010048191,0.210205609729445,340.915114789846));
#22657=CARTESIAN_POINT('Ctrl Pts',(154.478408717945,0.0526084993023518,
340.916516112401));
#22658=CARTESIAN_POINT('Ctrl Pts',(154.485806167149,-0.104962612495201,
340.917917203781));
#22659=CARTESIAN_POINT('Ctrl Pts',(154.493203616353,-0.262636786066086,
340.913019618621));
#22660=CARTESIAN_POINT('Ctrl Pts',(154.500601065557,-0.419873538320556,
340.9018333401));
#22661=CARTESIAN_POINT('Ctrl Pts',(154.507998194021,-0.577103473063572,
340.890647546597));
#22662=CARTESIAN_POINT('Ctrl Pts',(154.515395322484,-0.733895651930085,
340.873173628371));
#22663=CARTESIAN_POINT('Ctrl Pts',(154.522792450948,-0.889712990194715,
340.849473596622));
#22664=CARTESIAN_POINT('Ctrl Pts',(154.530190718384,-1.04555432043963,340.82576991566));
#22665=CARTESIAN_POINT('Ctrl Pts',(154.537588985821,-1.20042014222144,340.795838268471));
#22666=CARTESIAN_POINT('Ctrl Pts',(154.544987253258,-1.35378200875829,340.759792082642));
#22667=CARTESIAN_POINT('Ctrl Pts',(154.552388119783,-1.50719775293166,340.723733233409));
#22668=CARTESIAN_POINT('Ctrl Pts',(154.559788986309,-1.65910812682363,340.681555654008));
#22669=CARTESIAN_POINT('Ctrl Pts',(154.567189852835,-1.8089984689459,340.633423035939));
#22670=CARTESIAN_POINT('Ctrl Pts',(154.57459884622,-1.95905340499408,340.585237563654));
#22671=CARTESIAN_POINT('Ctrl Pts',(154.582007839605,-2.10708352388084,340.53108410774));
#22672=CARTESIAN_POINT('Ctrl Pts',(154.589416832989,-2.25259213688343,340.471175305851));
#22673=CARTESIAN_POINT('Ctrl Pts',(154.59683039057,-2.3981903882106,340.411229598073));
#22674=CARTESIAN_POINT('Ctrl Pts',(154.60424394815,-2.54126370006746,340.345521634857));
#22675=CARTESIAN_POINT('Ctrl Pts',(154.61165750573,-2.68133920022774,340.274310443634));
#22676=CARTESIAN_POINT('Ctrl Pts',(154.619081617867,-2.82161412350682,340.202997870243));
#22677=CARTESIAN_POINT('Ctrl Pts',(154.626505730004,-2.95888238638172,340.126166602868));
#22678=CARTESIAN_POINT('Ctrl Pts',(154.63392984214,-3.09269865372623,340.044119903387));
#22679=CARTESIAN_POINT('Ctrl Pts',(154.637786967295,-3.16222159213994,340.001493339753));
#22680=CARTESIAN_POINT('Ctrl Pts',(154.641644092449,-3.23081327474718,339.957459704203));
#22681=CARTESIAN_POINT('Ctrl Pts',(154.645501217604,-3.29841479654227,339.912065796836));
#22682=CARTESIAN_POINT('Ctrl Pts',(154.652900495726,-3.42809751130321,339.824984840898));
#22683=CARTESIAN_POINT('Ctrl Pts',(154.660299773847,-3.5545314263883,339.732628997538));
#22684=CARTESIAN_POINT('Ctrl Pts',(154.667699051969,-3.67725610131445,339.635268938028));
#22685=CARTESIAN_POINT('Ctrl Pts',(154.675089582152,-3.79983568263393,339.53802398432));
#22686=CARTESIAN_POINT('Ctrl Pts',(154.682480112335,-3.91871446016488,339.435786820934));
#22687=CARTESIAN_POINT('Ctrl Pts',(154.689870642517,-4.03345957138276,339.32887219129));
#22688=CARTESIAN_POINT('Ctrl Pts',(154.697254074777,-4.14809448049912,339.222060243291));
#22689=CARTESIAN_POINT('Ctrl Pts',(154.704637507037,-4.25860335270168,339.11058002586));
#22690=CARTESIAN_POINT('Ctrl Pts',(154.712020939297,-4.36458525258753,338.994787370486));
#22691=CARTESIAN_POINT('Ctrl Pts',(154.719398917832,-4.47048886961645,338.879080244621));
#22692=CARTESIAN_POINT('Ctrl Pts',(154.726776896366,-4.57187191886398,338.759067298811));
#22693=CARTESIAN_POINT('Ctrl Pts',(154.734154874901,-4.66836941033831,338.635142034518));
#22694=CARTESIAN_POINT('Ctrl Pts',(154.741827655959,-4.76872266038726,338.506265077769));
#22695=CARTESIAN_POINT('Ctrl Pts',(154.749500437017,-4.86379154784705,338.373156971735));
#22696=CARTESIAN_POINT('Ctrl Pts',(154.757173218075,-4.95321046000594,338.236299847262));
#22697=CARTESIAN_POINT('Ctrl Pts',(154.764546233667,-5.03913589285325,338.104789550674));
#22698=CARTESIAN_POINT('Ctrl Pts',(154.771919249259,-5.11984426264736,337.969817982963));
#22699=CARTESIAN_POINT('Ctrl Pts',(154.779292264851,-5.19505466459128,337.831843497513));
#22700=CARTESIAN_POINT('Ctrl Pts',(154.786665137011,-5.27026360342517,337.693871696158));
#22701=CARTESIAN_POINT('Ctrl Pts',(154.794038009172,-5.33997460689103,337.552897423265));
#22702=CARTESIAN_POINT('Ctrl Pts',(154.801410881332,-5.40395247186991,337.409404126391));
#22703=CARTESIAN_POINT('Ctrl Pts',(154.808785090685,-5.46794194029385,337.265884804632));
#22704=CARTESIAN_POINT('Ctrl Pts',(154.816159300038,-5.52619604719842,337.119845892829));
#22705=CARTESIAN_POINT('Ctrl Pts',(154.823533509391,-5.57852760379302,336.971791149239));
#22706=CARTESIAN_POINT('Ctrl Pts',(154.830910537117,-5.63087916115778,336.82367982012));
#22707=CARTESIAN_POINT('Ctrl Pts',(154.838287564843,-5.67730353701384,336.673551479729));
#22708=CARTESIAN_POINT('Ctrl Pts',(154.84566459257,-5.71766335604758,336.521925198363));
#22709=CARTESIAN_POINT('Ctrl Pts',(154.853049733589,-5.75806756301706,336.370132157635));
#22710=CARTESIAN_POINT('Ctrl Pts',(154.860434874608,-5.79239379978253,336.216838250088));
#22711=CARTESIAN_POINT('Ctrl Pts',(154.867820015627,-5.82055564983954,336.062573521984));
#22712=CARTESIAN_POINT('Ctrl Pts',(154.875209958905,-5.84873581240917,335.908208481763));
#22713=CARTESIAN_POINT('Ctrl Pts',(154.882599902183,-5.87074355018513,335.752871734394));
#22714=CARTESIAN_POINT('Ctrl Pts',(154.889989845461,-5.88654436198352,335.597098012809));
#22715=CARTESIAN_POINT('Ctrl Pts',(154.89738978996,-5.90236655789945,335.441113473981));
#22716=CARTESIAN_POINT('Ctrl Pts',(154.904789734459,-5.91196503569743,335.284691153918));
#22717=CARTESIAN_POINT('Ctrl Pts',(154.912189678958,-5.91535736389914,335.128365960691));
#22718=CARTESIAN_POINT('Ctrl Pts',(154.914226992737,-5.91629132184814,335.085327331125));
#22719=CARTESIAN_POINT('Ctrl Pts',(154.916264306515,-5.91675516787735,335.042296033567));
#22720=CARTESIAN_POINT('Ctrl Pts',(154.918301620294,-5.91674995657411,334.999283145596));
#22721=CARTESIAN_POINT('',(156.668300924438,-5.91517048090566,335.005379803398));
#22722=CARTESIAN_POINT('Ctrl Pts',(154.918301620294,-5.92639295407506,334.999281977281));
#22723=CARTESIAN_POINT('Ctrl Pts',(154.920114164155,-5.92645845110932,334.960952179359));
#22724=CARTESIAN_POINT('Ctrl Pts',(154.921926708016,-5.92611884753196,334.922623573182));
#22725=CARTESIAN_POINT('Ctrl Pts',(155.016485263302,-5.88708407117718,332.923475726914));
#22726=CARTESIAN_POINT('Ctrl Pts',(155.201977286152,-3.67068872424052,329.043602833008));
#22727=CARTESIAN_POINT('Ctrl Pts',(155.480215320426,3.02244115912318,328.68989125602));
#22728=CARTESIAN_POINT('Ctrl Pts',(155.7584533547,6.94192140191797,334.126873336331));
#22729=CARTESIAN_POINT('Ctrl Pts',(156.036691388974,4.49090283676372,340.365110868564));
#22730=CARTESIAN_POINT('Ctrl Pts',(156.314929423248,-2.08135097606897,341.67986534562));
#22731=CARTESIAN_POINT('Ctrl Pts',(156.525465843093,-5.609153889735,338.036267632335));
#22732=CARTESIAN_POINT('Ctrl Pts',(156.643256251513,-5.91922902505516,335.537755193878));
#22733=CARTESIAN_POINT('Ctrl Pts',(156.668300648508,-5.91454511534654,335.0053851016));
#22734=CARTESIAN_POINT('',(158.418302357817,-5.91166820494994,334.998075736246));
#22735=CARTESIAN_POINT('Ctrl Pts',(156.668301620294,-5.91674756634078,335.005366442065));
#22736=CARTESIAN_POINT('Ctrl Pts',(156.675633488304,-5.91688897598109,334.849455852701));
#22737=CARTESIAN_POINT('Ctrl Pts',(156.682965356315,-5.9108636352077,334.693405342462));
#22738=CARTESIAN_POINT('Ctrl Pts',(156.690297224325,-5.89866525491898,334.537745986592));
#22739=CARTESIAN_POINT('Ctrl Pts',(156.697843402136,-5.88611031714083,334.377536722634));
#22740=CARTESIAN_POINT('Ctrl Pts',(156.705389579948,-5.86701591486274,334.217742239667));
#22741=CARTESIAN_POINT('Ctrl Pts',(156.712935757759,-5.84143288569137,334.058940807142));
#22742=CARTESIAN_POINT('Ctrl Pts',(156.720262482015,-5.81659384729707,333.904757545529));
#22743=CARTESIAN_POINT('Ctrl Pts',(156.727589206272,-5.78563839821375,333.751510778622));
#22744=CARTESIAN_POINT('Ctrl Pts',(156.734915930528,-5.74866554615006,333.599723241281));
#22745=CARTESIAN_POINT('Ctrl Pts',(156.742242472371,-5.71169361460261,333.447939483008));
#22746=CARTESIAN_POINT('Ctrl Pts',(156.749569014213,-5.6687046679693,333.297615252379));
#22747=CARTESIAN_POINT('Ctrl Pts',(156.756895556055,-5.61984841418772,333.149261130237));
#22748=CARTESIAN_POINT('Ctrl Pts',(156.764223429155,-5.57098328306163,333.000880051655));
#22749=CARTESIAN_POINT('Ctrl Pts',(156.771551302255,-5.51624884236344,332.854470155897));
#22750=CARTESIAN_POINT('Ctrl Pts',(156.778879175354,-5.45584397225896,332.710524707959));
#22751=CARTESIAN_POINT('Ctrl Pts',(156.786589701724,-5.3922848279483,332.559062591039));
#22752=CARTESIAN_POINT('Ctrl Pts',(156.794300228094,-5.32244733029172,332.410329655211));
#22753=CARTESIAN_POINT('Ctrl Pts',(156.802010754465,-5.24661907655998,332.264873160532));
#22754=CARTESIAN_POINT('Ctrl Pts',(156.809349811636,-5.17444399244361,332.126424307736));
#22755=CARTESIAN_POINT('Ctrl Pts',(156.816688868807,-5.09684209173963,331.990943901949));
#22756=CARTESIAN_POINT('Ctrl Pts',(156.824027925979,-5.01410656628233,331.858875057489));
#22757=CARTESIAN_POINT('Ctrl Pts',(156.831371939168,-4.93131517006361,331.726717027799));
#22758=CARTESIAN_POINT('Ctrl Pts',(156.838715952357,-4.84338345930787,331.597975460644));
#22759=CARTESIAN_POINT('Ctrl Pts',(156.846059965546,-4.75064585436508,331.473061592698));
#22760=CARTESIAN_POINT('Ctrl Pts',(156.853413787207,-4.65778439148889,331.347980893038));
#22761=CARTESIAN_POINT('Ctrl Pts',(156.860767608869,-4.56010446362926,331.226738388744));
#22762=CARTESIAN_POINT('Ctrl Pts',(156.868121430531,-4.45797865208204,331.109709920831));
#22763=CARTESIAN_POINT('Ctrl Pts',(156.869216117619,-4.44277624272213,331.092289107728));
#22764=CARTESIAN_POINT('Ctrl Pts',(156.870310804708,-4.42747537810144,331.074961603319));
#22765=CARTESIAN_POINT('Ctrl Pts',(156.871405491796,-4.41207735084086,331.057728571915));
#22766=CARTESIAN_POINT('Ctrl Pts',(156.878829469234,-4.30765060806387,330.940857150189));
#22767=CARTESIAN_POINT('Ctrl Pts',(156.886253446672,-4.1984194186915,330.827961524164));
#22768=CARTESIAN_POINT('Ctrl Pts',(156.89367742411,-4.08471836925703,330.719461902242));
#22769=CARTESIAN_POINT('Ctrl Pts',(156.901092640137,-3.97115150416818,330.611090326199));
#22770=CARTESIAN_POINT('Ctrl Pts',(156.908507856165,-3.85312554658059,330.507104682716));
#22771=CARTESIAN_POINT('Ctrl Pts',(156.915923072193,-3.73101483348997,330.40789167432));
#22772=CARTESIAN_POINT('Ctrl Pts',(156.923331153337,-3.60902161471262,330.308774128182));
#22773=CARTESIAN_POINT('Ctrl Pts',(156.930739234481,-3.4829517527098,330.214420308675));
#22774=CARTESIAN_POINT('Ctrl Pts',(156.938147315625,-3.3532157951102,330.125179552648));
#22775=CARTESIAN_POINT('Ctrl Pts',(156.945549882799,-3.22357640235326,330.036005220145));
#22776=CARTESIAN_POINT('Ctrl Pts',(156.952952449973,-3.09027665349441,329.951936583933));
#22777=CARTESIAN_POINT('Ctrl Pts',(156.960355017147,-2.95375938919286,329.873282138321));
#22778=CARTESIAN_POINT('Ctrl Pts',(156.967753686902,-2.81731400063397,329.794669103931));
#22779=CARTESIAN_POINT('Ctrl Pts',(156.975152356656,-2.67765479291337,329.721464768953));
#22780=CARTESIAN_POINT('Ctrl Pts',(156.982551026411,-2.53525264600912,329.653933728113));
#22781=CARTESIAN_POINT('Ctrl Pts',(156.989948475615,-2.39287399103746,329.586413827799));
#22782=CARTESIAN_POINT('Ctrl Pts',(156.997345924819,-2.24775363183439,329.524565523891));
#22783=CARTESIAN_POINT('Ctrl Pts',(157.004743374023,-2.10038615785365,329.468606997293));
#22784=CARTESIAN_POINT('Ctrl Pts',(157.012140502486,-1.95302507346984,329.412650896959));
#22785=CARTESIAN_POINT('Ctrl Pts',(157.01953763095,-1.80341741693734,329.36258419866));
#22786=CARTESIAN_POINT('Ctrl Pts',(157.026934759413,-1.65207656878288,329.318576448338));
#22787=CARTESIAN_POINT('Ctrl Pts',(157.03433302685,-1.50071241791526,329.274561921921));
#22788=CARTESIAN_POINT('Ctrl Pts',(157.041731294287,-1.34761490244525,329.236608305275));
#22789=CARTESIAN_POINT('Ctrl Pts',(157.049129561723,-1.19331118283358,329.204834861419));
#22790=CARTESIAN_POINT('Ctrl Pts',(157.056530428249,-1.03895325470312,329.173050255218));
#22791=CARTESIAN_POINT('Ctrl Pts',(157.063931294775,-0.883388644052891,
329.147450219807));
#22792=CARTESIAN_POINT('Ctrl Pts',(157.0713321613,-0.727153136431057,329.128102616813));
#22793=CARTESIAN_POINT('Ctrl Pts',(157.078741154685,-0.570746067284901,
329.108733768302));
#22794=CARTESIAN_POINT('Ctrl Pts',(157.08615014807,-0.41366700052293,329.095631109409));
#22795=CARTESIAN_POINT('Ctrl Pts',(157.093559141454,-0.256455993363195,
329.088810535436));
#22796=CARTESIAN_POINT('Ctrl Pts',(157.100972699035,-0.0991481388001783,
329.081985759755));
#22797=CARTESIAN_POINT('Ctrl Pts',(157.108386256615,0.0582914457842649,
329.081450781708));
#22798=CARTESIAN_POINT('Ctrl Pts',(157.115799814195,0.215324808441732,329.087169392806));
#22799=CARTESIAN_POINT('Ctrl Pts',(157.123223926332,0.372581736839745,329.092896145394));
#22800=CARTESIAN_POINT('Ctrl Pts',(157.130648038468,0.529430917147036,329.104894240069));
#22801=CARTESIAN_POINT('Ctrl Pts',(157.138072150605,0.685340784651717,329.123075755857));
#22802=CARTESIAN_POINT('Ctrl Pts',(157.14192927576,0.766342237857799,329.132521785309));
#22803=CARTESIAN_POINT('Ctrl Pts',(157.145786400915,0.847090326754616,329.143636015974));
#22804=CARTESIAN_POINT('Ctrl Pts',(157.14964352607,0.92751192906392,329.156400750912));
#22805=CARTESIAN_POINT('Ctrl Pts',(157.157067503508,1.08230290345749,329.180969594383));
#22806=CARTESIAN_POINT('Ctrl Pts',(157.164491480946,1.23635050815835,329.21173013068));
#22807=CARTESIAN_POINT('Ctrl Pts',(157.171915458384,1.38912031698442,329.248628397726));
#22808=CARTESIAN_POINT('Ctrl Pts',(157.179330674411,1.5417098344505,329.285483119266));
#22809=CARTESIAN_POINT('Ctrl Pts',(157.186745890439,1.69302419847087,329.328461066591));
#22810=CARTESIAN_POINT('Ctrl Pts',(157.194161106466,1.84253564741217,329.377456718662));
#22811=CARTESIAN_POINT('Ctrl Pts',(157.20156918761,1.99190323719024,329.426405227364));
#22812=CARTESIAN_POINT('Ctrl Pts',(157.208977268755,2.13947101318137,329.481359798149));
#22813=CARTESIAN_POINT('Ctrl Pts',(157.216385349899,2.28472303969744,329.54216423897));
#22814=CARTESIAN_POINT('Ctrl Pts',(157.223787917073,2.42986695247754,329.602923421936));
#22815=CARTESIAN_POINT('Ctrl Pts',(157.231190484247,2.57269820504026,329.669523661665));
#22816=CARTESIAN_POINT('Ctrl Pts',(157.238593051421,2.71271773144703,329.741759507973));
#22817=CARTESIAN_POINT('Ctrl Pts',(157.245991721175,2.85266353818495,329.813957322424));
#22818=CARTESIAN_POINT('Ctrl Pts',(157.25339039093,2.98980023615567,329.891784663573));
#22819=CARTESIAN_POINT('Ctrl Pts',(157.260789060685,3.12365050183226,329.974988745793));
#22820=CARTESIAN_POINT('Ctrl Pts',(157.268186509889,3.25747868637105,330.058179101923));
#22821=CARTESIAN_POINT('Ctrl Pts',(157.275583959093,3.38802119797191,330.146744241885));
#22822=CARTESIAN_POINT('Ctrl Pts',(157.282981408297,3.51482691292582,330.24038632506));
#22823=CARTESIAN_POINT('Ctrl Pts',(157.29037853676,3.64162712980491,330.334024348078));
#22824=CARTESIAN_POINT('Ctrl Pts',(157.297775665224,3.76469057196565,330.43273865492));
#22825=CARTESIAN_POINT('Ctrl Pts',(157.305172793687,3.88359684494801,330.536189283985));
#22826=CARTESIAN_POINT('Ctrl Pts',(157.312571061124,4.0025214265282,330.639655841865));
#22827=CARTESIAN_POINT('Ctrl Pts',(157.31996932856,4.11728728282484,330.74785992907));
#22828=CARTESIAN_POINT('Ctrl Pts',(157.327367595997,4.2275088462469,330.860422785186));
#22829=CARTESIAN_POINT('Ctrl Pts',(157.334768462523,4.33776913166372,330.973025185818));
#22830=CARTESIAN_POINT('Ctrl Pts',(157.342169329049,4.44348168471309,331.089989137649));
#22831=CARTESIAN_POINT('Ctrl Pts',(157.349570195574,4.54429949479953,331.210900811002));
#22832=CARTESIAN_POINT('Ctrl Pts',(157.356979188959,4.6452280124797,331.331945256932));
#22833=CARTESIAN_POINT('Ctrl Pts',(157.364388182344,4.74125081409529,331.45694579475));
#22834=CARTESIAN_POINT('Ctrl Pts',(157.371797175728,4.83206227699911,331.585456880679));
#22835=CARTESIAN_POINT('Ctrl Pts',(157.379210733309,4.9229296828966,331.71404713387));
#22836=CARTESIAN_POINT('Ctrl Pts',(157.386624290889,5.00857915044992,331.846151932055));
#22837=CARTESIAN_POINT('Ctrl Pts',(157.394037848469,5.08875001148244,331.981299305473));
#22838=CARTESIAN_POINT('Ctrl Pts',(157.401461960606,5.16903501041282,332.116639085919));
#22839=CARTESIAN_POINT('Ctrl Pts',(157.408886072742,5.24382564810089,332.255029765349));
#22840=CARTESIAN_POINT('Ctrl Pts',(157.416310184879,5.31290819900202,332.395976760573));
#22841=CARTESIAN_POINT('Ctrl Pts',(157.420167310034,5.34879936550541,332.469204399213));
#22842=CARTESIAN_POINT('Ctrl Pts',(157.424024435189,5.3831505960538,332.543121737798));
#22843=CARTESIAN_POINT('Ctrl Pts',(157.427881560343,5.41593720172094,332.617657709414));
#22844=CARTESIAN_POINT('Ctrl Pts',(157.435305537781,5.47904301524107,332.761120353065));
#22845=CARTESIAN_POINT('Ctrl Pts',(157.442729515219,5.53653982217527,332.907308561549));
#22846=CARTESIAN_POINT('Ctrl Pts',(157.450153492657,5.58818379171178,333.055743722512));
#22847=CARTESIAN_POINT('Ctrl Pts',(157.457568708685,5.63976681359408,333.204003707653));
#22848=CARTESIAN_POINT('Ctrl Pts',(157.464983924713,5.68551062558205,333.354505017881));
#22849=CARTESIAN_POINT('Ctrl Pts',(157.47239914074,5.72521836046588,333.506746743689));
#22850=CARTESIAN_POINT('Ctrl Pts',(157.479807221884,5.76488788876708,333.658841983275));
#22851=CARTESIAN_POINT('Ctrl Pts',(157.487215303028,5.79853280881599,333.81267394587));
#22852=CARTESIAN_POINT('Ctrl Pts',(157.494623384173,5.82600526343079,333.96772424567));
#22853=CARTESIAN_POINT('Ctrl Pts',(157.502025951347,5.85345726979598,334.122659138701));
#22854=CARTESIAN_POINT('Ctrl Pts',(157.509428518521,5.87474589377109,334.278810197391));
#22855=CARTESIAN_POINT('Ctrl Pts',(157.516831085695,5.88977382958386,334.435646565662));
#22856=CARTESIAN_POINT('Ctrl Pts',(157.524229755449,5.90479385325413,334.592400360271));
#22857=CARTESIAN_POINT('Ctrl Pts',(157.531628425204,5.9135597178815,334.749838375306));
#22858=CARTESIAN_POINT('Ctrl Pts',(157.539027094959,5.91602568914555,334.907422422423));
#22859=CARTESIAN_POINT('Ctrl Pts',(157.546424544163,5.9184912536009,335.064980473065));
#22860=CARTESIAN_POINT('Ctrl Pts',(157.553821993367,5.91465898150763,335.222684135173));
#22861=CARTESIAN_POINT('Ctrl Pts',(157.561219442571,5.90453520447066,335.379992870547));
#22862=CARTESIAN_POINT('Ctrl Pts',(157.568616571034,5.894411866383,335.537294785289));
#22863=CARTESIAN_POINT('Ctrl Pts',(157.576013699498,5.87799758971425,335.694201434904));
#22864=CARTESIAN_POINT('Ctrl Pts',(157.583410827961,5.85535075586203,335.850175327992));
#22865=CARTESIAN_POINT('Ctrl Pts',(157.590809095398,5.83270043496279,336.006173237166));
#22866=CARTESIAN_POINT('Ctrl Pts',(157.598207362834,5.80381569970409,336.161237734484));
#22867=CARTESIAN_POINT('Ctrl Pts',(157.605605630271,5.76880640505196,336.314839618939));
#22868=CARTESIAN_POINT('Ctrl Pts',(157.613006496796,5.73378481126629,336.468495465352));
#22869=CARTESIAN_POINT('Ctrl Pts',(157.620407363322,5.69263445709513,336.620687312216));
#22870=CARTESIAN_POINT('Ctrl Pts',(157.627808229848,5.64551555339729,336.770899403933));
#22871=CARTESIAN_POINT('Ctrl Pts',(157.635217223233,5.59834490863842,336.921276442887));
#22872=CARTESIAN_POINT('Ctrl Pts',(157.642626216617,5.54519273735874,337.069669028866));
#22873=CARTESIAN_POINT('Ctrl Pts',(157.650035210002,5.48626831687429,337.21557904796));
#22874=CARTESIAN_POINT('Ctrl Pts',(157.657448767582,5.42730759691433,337.36157895266));
#22875=CARTESIAN_POINT('Ctrl Pts',(157.664862325163,5.36256769524638,337.505092903647));
#22876=CARTESIAN_POINT('Ctrl Pts',(157.672275882743,5.29230443880382,337.64564628957));
#22877=CARTESIAN_POINT('Ctrl Pts',(157.67969999488,5.22194114975245,337.78639977897));
#22878=CARTESIAN_POINT('Ctrl Pts',(157.687124107016,5.14603898052259,337.924183959286));
#22879=CARTESIAN_POINT('Ctrl Pts',(157.694548219153,5.06489817751462,338.058551456803));
#22880=CARTESIAN_POINT('Ctrl Pts',(157.698405344307,5.02274226357107,338.128360781484));
#22881=CARTESIAN_POINT('Ctrl Pts',(157.702262469462,4.97917301852347,338.197248377384));
#22882=CARTESIAN_POINT('Ctrl Pts',(157.706119594616,4.93423684346073,338.265155024671));
#22883=CARTESIAN_POINT('Ctrl Pts',(157.713543572054,4.8477462224802,338.395857917928));
#22884=CARTESIAN_POINT('Ctrl Pts',(157.720967549492,4.75592826057564,338.523319037407));
#22885=CARTESIAN_POINT('Ctrl Pts',(157.72839152693,4.65905348224265,338.647074335972));
#22886=CARTESIAN_POINT('Ctrl Pts',(157.735806742958,4.56229303072363,338.770683584664));
#22887=CARTESIAN_POINT('Ctrl Pts',(157.743221958986,4.46048786959514,338.890595426793));
#22888=CARTESIAN_POINT('Ctrl Pts',(157.750637175013,4.35395268820359,339.006373241647));
#22889=CARTESIAN_POINT('Ctrl Pts',(157.758045256157,4.24752001442733,339.12203965567));
#22890=CARTESIAN_POINT('Ctrl Pts',(157.765453337302,4.13636663200349,339.233579688559));
#22891=CARTESIAN_POINT('Ctrl Pts',(157.772861418446,4.02084844861,339.34058847575));
#22892=CARTESIAN_POINT('Ctrl Pts',(157.78026398562,3.90541624751008,339.447517614346));
#22893=CARTESIAN_POINT('Ctrl Pts',(157.787666552794,3.78562598689547,339.549921970222));
#22894=CARTESIAN_POINT('Ctrl Pts',(157.795069119968,3.66187141723115,339.647432440194));
#22895=CARTESIAN_POINT('Ctrl Pts',(157.802467789722,3.53818200380669,339.744891571329));
#22896=CARTESIAN_POINT('Ctrl Pts',(157.809866459477,3.41053273050614,339.837461717633));
#22897=CARTESIAN_POINT('Ctrl Pts',(157.817265129232,3.27935142192641,339.924813175544));
#22898=CARTESIAN_POINT('Ctrl Pts',(157.824662578436,3.1481917541891,340.012150223176));
#22899=CARTESIAN_POINT('Ctrl Pts',(157.83206002764,3.01350151793727,340.094270084416));
#22900=CARTESIAN_POINT('Ctrl Pts',(157.839457476844,2.87573868966934,340.170885567409));
#22901=CARTESIAN_POINT('Ctrl Pts',(157.846854605307,2.73798183455781,340.247497728488));
#22902=CARTESIAN_POINT('Ctrl Pts',(157.854251733771,2.59715297848425,340.318605804462));
#22903=CARTESIAN_POINT('Ctrl Pts',(157.861648862234,2.45373570295703,340.383968022057));
#22904=CARTESIAN_POINT('Ctrl Pts',(157.869047129671,2.31029634474955,340.449340303802));
#22905=CARTESIAN_POINT('Ctrl Pts',(157.876445397108,2.16426811314458,340.508964810792));
#22906=CARTESIAN_POINT('Ctrl Pts',(157.883843664544,2.0161554733843,340.562647541382));
#22907=CARTESIAN_POINT('Ctrl Pts',(157.89124453107,1.8679908000963,340.616349131279));
#22908=CARTESIAN_POINT('Ctrl Pts',(157.898645397596,1.7177406113502,340.664104661657));
#22909=CARTESIAN_POINT('Ctrl Pts',(157.906046264121,1.56592531631867,340.705769752296));
#22910=CARTESIAN_POINT('Ctrl Pts',(157.913455257506,1.41394331357857,340.747480595188));
#22911=CARTESIAN_POINT('Ctrl Pts',(157.920864250891,1.26039313246243,340.783087543445));
#22912=CARTESIAN_POINT('Ctrl Pts',(157.928273244276,1.10580689954551,340.812497024809));
#22913=CARTESIAN_POINT('Ctrl Pts',(157.935686801856,0.951125436176458,340.841924623429));
#22914=CARTESIAN_POINT('Ctrl Pts',(157.943100359436,0.795407017488464,340.865147092659));
#22915=CARTESIAN_POINT('Ctrl Pts',(157.950513917017,0.639189196924143,340.882122723391));
#22916=CARTESIAN_POINT('Ctrl Pts',(157.957938029153,0.482748971693086,340.899122522041));
#22917=CARTESIAN_POINT('Ctrl Pts',(157.96536214129,0.32580829593344,340.909857694657));
#22918=CARTESIAN_POINT('Ctrl Pts',(157.972786253427,0.168905856300576,340.914338625257));
#22919=CARTESIAN_POINT('Ctrl Pts',(157.976643378581,0.0873887219144972,
340.916666649109));
#22920=CARTESIAN_POINT('Ctrl Pts',(157.980500503736,0.00588185436856069,
340.91730737235));
#22921=CARTESIAN_POINT('Ctrl Pts',(157.984357628891,-0.0755398368275449,
340.916267767398));
#22922=CARTESIAN_POINT('Ctrl Pts',(157.991781606329,-0.232255726034468,
340.914266794291));
#22923=CARTESIAN_POINT('Ctrl Pts',(157.999205583767,-0.389128468368965,
340.906031636743));
#22924=CARTESIAN_POINT('Ctrl Pts',(158.006629561205,-0.545621440364771,
340.89153866204));
#22925=CARTESIAN_POINT('Ctrl Pts',(158.014044777232,-0.701929727107513,
340.877062791229));
#22926=CARTESIAN_POINT('Ctrl Pts',(158.02145999326,-0.857858767626078,340.856343837634));
#22927=CARTESIAN_POINT('Ctrl Pts',(158.028875209288,-1.01287110178623,340.829410149721));
#22928=CARTESIAN_POINT('Ctrl Pts',(158.036283290432,-1.1677342838595,340.802502377266));
#22929=CARTESIAN_POINT('Ctrl Pts',(158.043691371576,-1.32168215032732,340.769391838594));
#22930=CARTESIAN_POINT('Ctrl Pts',(158.05109945272,-1.47418163987487,340.730158728618));
#22931=CARTESIAN_POINT('Ctrl Pts',(158.058502019894,-1.62656762126736,340.690954820562));
#22932=CARTESIAN_POINT('Ctrl Pts',(158.065904587068,-1.77750701240742,340.645637507723));
#22933=CARTESIAN_POINT('Ctrl Pts',(158.073307154242,-1.9264763455828,340.594338160356));
#22934=CARTESIAN_POINT('Ctrl Pts',(158.080705823997,-2.07536724705518,340.54306582187));
#22935=CARTESIAN_POINT('Ctrl Pts',(158.088104493752,-2.22228980427606,340.485817842513));
#22936=CARTESIAN_POINT('Ctrl Pts',(158.095503163506,-2.36673524204908,340.422775567598));
#22937=CARTESIAN_POINT('Ctrl Pts',(158.10290061271,-2.51115685081043,340.359743692702));
#22938=CARTESIAN_POINT('Ctrl Pts',(158.110298061914,-2.65310180943753,340.290919568501));
#22939=CARTESIAN_POINT('Ctrl Pts',(158.117695511118,-2.79208077481128,340.216532901212));
#22940=CARTESIAN_POINT('Ctrl Pts',(158.125092639582,-2.93105371429922,340.1421494592));
#22941=CARTESIAN_POINT('Ctrl Pts',(158.132489768045,-3.06706058718992,340.062204129766));
#22942=CARTESIAN_POINT('Ctrl Pts',(158.139886896509,-3.19963638747686,339.976972729525));
#22943=CARTESIAN_POINT('Ctrl Pts',(158.147285163945,-3.33223260112725,339.891728205776));
#22944=CARTESIAN_POINT('Ctrl Pts',(158.154683431382,-3.46139637630798,339.80119619243));
#22945=CARTESIAN_POINT('Ctrl Pts',(158.162081698818,-3.58669157780754,339.705695919647));
#22946=CARTESIAN_POINT('Ctrl Pts',(158.169482565344,-3.712030796829,339.610162096615));
#22947=CARTESIAN_POINT('Ctrl Pts',(158.17688343187,-3.83349843962747,339.509656765149));
#22948=CARTESIAN_POINT('Ctrl Pts',(158.184284298396,-3.95069147053294,339.404539416007));
#22949=CARTESIAN_POINT('Ctrl Pts',(158.19169329178,-4.06801319059056,339.299306637965));
#22950=CARTESIAN_POINT('Ctrl Pts',(158.199102285165,-4.18105064673004,339.189451977643));
#22951=CARTESIAN_POINT('Ctrl Pts',(158.20651127855,-4.28943718782086,339.075372274313));
#22952=CARTESIAN_POINT('Ctrl Pts',(158.21392483613,-4.39789049875953,338.961222293951));
#22953=CARTESIAN_POINT('Ctrl Pts',(158.22133839371,-4.50168694003735,338.842842364175));
#22954=CARTESIAN_POINT('Ctrl Pts',(158.228751951291,-4.6005005365625,338.720661953952));
#22955=CARTESIAN_POINT('Ctrl Pts',(158.236176063427,-4.69945481233254,338.598307597548));
#22956=CARTESIAN_POINT('Ctrl Pts',(158.243600175564,-4.79341185291784,338.472142253006));
#22957=CARTESIAN_POINT('Ctrl Pts',(158.251024287701,-4.88208887620064,338.342624532815));
#22958=CARTESIAN_POINT('Ctrl Pts',(158.254881412855,-4.92816015999168,338.275334862707));
#22959=CARTESIAN_POINT('Ctrl Pts',(158.25873853801,-4.97280700072594,338.207140731026));
#22960=CARTESIAN_POINT('Ctrl Pts',(158.262595663165,-5.01599472382435,338.138108903953));
#22961=CARTESIAN_POINT('Ctrl Pts',(158.27022228883,-5.10138904840625,338.001613487555));
#22962=CARTESIAN_POINT('Ctrl Pts',(158.277848914495,-5.18132210798116,337.86144817117));
#22963=CARTESIAN_POINT('Ctrl Pts',(158.285475540161,-5.25547266730665,337.718076085339));
#22964=CARTESIAN_POINT('Ctrl Pts',(158.293091648239,-5.32952096843845,337.574901718456));
#22965=CARTESIAN_POINT('Ctrl Pts',(158.300707756317,-5.39780249676258,337.428529695603));
#22966=CARTESIAN_POINT('Ctrl Pts',(158.308323864396,-5.46003945974696,337.279451613987));
#22967=CARTESIAN_POINT('Ctrl Pts',(158.315930634586,-5.52220011580696,337.130556312657));
#22968=CARTESIAN_POINT('Ctrl Pts',(158.323537404776,-5.57833083869148,336.978961879332));
#22969=CARTESIAN_POINT('Ctrl Pts',(158.331144174967,-5.62819983144839,336.825184160512));
#22970=CARTESIAN_POINT('Ctrl Pts',(158.338740327179,-5.6779992141233,336.671621093704));
#22971=CARTESIAN_POINT('Ctrl Pts',(158.34633647939,-5.72155418874964,336.515881145363));
#22972=CARTESIAN_POINT('Ctrl Pts',(158.353932631602,-5.7586812573137,336.358499443932));
#22973=CARTESIAN_POINT('Ctrl Pts',(158.361522571177,-5.79577796089941,336.201246459692));
#22974=CARTESIAN_POINT('Ctrl Pts',(158.369112510752,-5.82645715137391,336.042354732067));
#22975=CARTESIAN_POINT('Ctrl Pts',(158.376702450327,-5.85058504998213,335.882374713727));
#22976=CARTESIAN_POINT('Ctrl Pts',(158.384286117463,-5.87469300893786,335.722526905242));
#22977=CARTESIAN_POINT('Ctrl Pts',(158.3918697846,-5.89226041819555,335.561592939988));
#22978=CARTESIAN_POINT('Ctrl Pts',(158.399453451737,-5.90320452748765,335.400133564137));
#22979=CARTESIAN_POINT('Ctrl Pts',(158.405736174589,-5.91227122362711,335.266371824316));
#22980=CARTESIAN_POINT('Ctrl Pts',(158.412018897442,-5.91679300422876,335.132249777994));
#22981=CARTESIAN_POINT('Ctrl Pts',(158.418301620294,-5.91674969165613,334.998089820131));
#22982=CARTESIAN_POINT('',(160.168301620294,-5.92155652207472,334.995416553942));
#22983=CARTESIAN_POINT('Ctrl Pts',(158.418302957134,-5.90753895514141,334.998064291588));
#22984=CARTESIAN_POINT('Ctrl Pts',(158.459146537236,-5.91004580971049,334.127255823406));
#22985=CARTESIAN_POINT('Ctrl Pts',(158.592736128762,-5.32113314713912,331.282283490978));
#22986=CARTESIAN_POINT('Ctrl Pts',(158.819071731712,-0.92000436045686,328.064135605567));
#22987=CARTESIAN_POINT('Ctrl Pts',(159.097309765987,5.33464919017363,330.472954502217));
#22988=CARTESIAN_POINT('Ctrl Pts',(159.375547800261,6.69377391827487,337.0361762331));
#22989=CARTESIAN_POINT('Ctrl Pts',(159.653785834535,1.91012112151633,341.73082908878));
#22990=CARTESIAN_POINT('Ctrl Pts',(159.918037107879,-4.29783585754292,340.32320468228));
#22991=CARTESIAN_POINT('Ctrl Pts',(160.089542369799,-5.90729764126013,336.664520679854));
#22992=CARTESIAN_POINT('Ctrl Pts',(160.168301620294,-5.92155652207472,334.995416553942));
#22993=CARTESIAN_POINT('',(161.918301620294,-5.9222056262964,335.004340868688));
#22994=CARTESIAN_POINT('Ctrl Pts',(160.168301620294,-5.92155652207472,334.995416553942));
#22995=CARTESIAN_POINT('Ctrl Pts',(160.182288381224,-5.9240887396342,334.69900235207));
#22996=CARTESIAN_POINT('Ctrl Pts',(160.289021153575,-5.76896797440835,332.439729074422));
#22997=CARTESIAN_POINT('Ctrl Pts',(160.48849993736,-2.86034519230075,328.614778915175));
#22998=CARTESIAN_POINT('Ctrl Pts',(160.766737971629,3.82157172282052,329.139265192097));
#22999=CARTESIAN_POINT('Ctrl Pts',(161.044976005905,6.99648867421634,335.042061297929));
#23000=CARTESIAN_POINT('Ctrl Pts',(161.323214040178,3.75083123728682,340.906258371475));
#23001=CARTESIAN_POINT('Ctrl Pts',(161.601452074453,-2.93690866392185,341.350369313749));
#23002=CARTESIAN_POINT('Ctrl Pts',(161.799814601158,-5.78331565926206,337.512322992919));
#23003=CARTESIAN_POINT('Ctrl Pts',(161.905431116438,-5.9244497178173,335.277020989329));
#23004=CARTESIAN_POINT('Ctrl Pts',(161.918301620294,-5.9222056262964,335.004340868688));
#23005=CARTESIAN_POINT('',(163.668300761703,-5.91179366464294,335.002290923672));
#23006=CARTESIAN_POINT('Ctrl Pts',(161.918301620294,-5.9222056262964,335.004340868688));
#23007=CARTESIAN_POINT('Ctrl Pts',(161.998177127863,-5.90827859194964,333.312063450199));
#23008=CARTESIAN_POINT('Ctrl Pts',(162.170798646855,-4.25981713968337,329.631137126993));
#23009=CARTESIAN_POINT('Ctrl Pts',(162.436166177274,1.99090855870963,328.292623014017));
#23010=CARTESIAN_POINT('Ctrl Pts',(162.714404211547,6.71777126255143,333.044450924867));
#23011=CARTESIAN_POINT('Ctrl Pts',(162.992642245822,5.27983443289055,339.590857358107));
#23012=CARTESIAN_POINT('Ctrl Pts',(163.270880280096,-1.00332852560485,341.924301754756));
#23013=CARTESIAN_POINT('Ctrl Pts',(163.496099554182,-5.34393227885399,338.669603558887));
#23014=CARTESIAN_POINT('Ctrl Pts',(163.628572816844,-5.91070066925879,335.849222013648));
#23015=CARTESIAN_POINT('Ctrl Pts',(163.668300068081,-5.90778998552529,335.002304171406));
#23016=CARTESIAN_POINT('',(165.41830244586,-5.91482905803173,334.994703811423));
#23017=CARTESIAN_POINT('Ctrl Pts',(163.668301620294,-5.91674956281194,335.002274525151));
#23018=CARTESIAN_POINT('Ctrl Pts',(163.675857115675,-5.91681157553319,334.8409600894));
#23019=CARTESIAN_POINT('Ctrl Pts',(163.683412611056,-5.91027211048072,334.679685551574));
#23020=CARTESIAN_POINT('Ctrl Pts',(163.690968106437,-5.89716734275482,334.519013623846));
#23021=CARTESIAN_POINT('Ctrl Pts',(163.698527137371,-5.88405644272485,334.358266510572));
#23022=CARTESIAN_POINT('Ctrl Pts',(163.706086168305,-5.86437414400719,334.198122918836));
#23023=CARTESIAN_POINT('Ctrl Pts',(163.713645199238,-5.83820841926096,334.039139439996));
#23024=CARTESIAN_POINT('Ctrl Pts',(163.721208980901,-5.81202624977905,333.880056042606));
#23025=CARTESIAN_POINT('Ctrl Pts',(163.728772762564,-5.77935258811635,333.722134557066));
#23026=CARTESIAN_POINT('Ctrl Pts',(163.736336544226,-5.74032635561207,333.565920541405));
#23027=CARTESIAN_POINT('Ctrl Pts',(163.743921527928,-5.70119072866306,333.409268642186));
#23028=CARTESIAN_POINT('Ctrl Pts',(163.751506511629,-5.65566697243352,333.254334136229));
#23029=CARTESIAN_POINT('Ctrl Pts',(163.75909149533,-5.60394482166675,333.10164992738));
#23030=CARTESIAN_POINT('Ctrl Pts',(163.766672870695,-5.55224727621628,332.949038353626));
#23031=CARTESIAN_POINT('Ctrl Pts',(163.77425424606,-5.49435739914961,332.798675247789));
#23032=CARTESIAN_POINT('Ctrl Pts',(163.781835621425,-5.43051209425154,332.651070678652));
#23033=CARTESIAN_POINT('Ctrl Pts',(163.789431241455,-5.36654683025353,332.503188774929));
#23034=CARTESIAN_POINT('Ctrl Pts',(163.797026861485,-5.29660392036394,332.35807608578));
#23035=CARTESIAN_POINT('Ctrl Pts',(163.804622481514,-5.22096663919529,332.216218773878));
#23036=CARTESIAN_POINT('Ctrl Pts',(163.812200437224,-5.14550525955161,332.074691364335));
#23037=CARTESIAN_POINT('Ctrl Pts',(163.819778392934,-5.06437620414303,331.93640446396));
#23038=CARTESIAN_POINT('Ctrl Pts',(163.827356348643,-4.97790233694105,331.801810060929));
#23039=CARTESIAN_POINT('Ctrl Pts',(163.834780326081,-4.89318555266768,331.669950513358));
#23040=CARTESIAN_POINT('Ctrl Pts',(163.842204303519,-4.80309811376579,331.541260465337));
#23041=CARTESIAN_POINT('Ctrl Pts',(163.849628280957,-4.70790425024316,331.416207576736));
#23042=CARTESIAN_POINT('Ctrl Pts',(163.857043496985,-4.61282272980215,331.291302269359));
#23043=CARTESIAN_POINT('Ctrl Pts',(163.864458713012,-4.51264700414154,331.170025871393));
#23044=CARTESIAN_POINT('Ctrl Pts',(163.87187392904,-4.40768583465019,331.0528192155));
#23045=CARTESIAN_POINT('Ctrl Pts',(163.879282010184,-4.30282565826751,330.935725335262));
#23046=CARTESIAN_POINT('Ctrl Pts',(163.886690091328,-4.19318945212747,330.822693677464));
#23047=CARTESIAN_POINT('Ctrl Pts',(163.894098172472,-4.07912762124907,330.714133878425));
#23048=CARTESIAN_POINT('Ctrl Pts',(163.901500739646,-3.96515068867476,330.605654882427));
#23049=CARTESIAN_POINT('Ctrl Pts',(163.908903306821,-3.84675495952377,330.501641373885));
#23050=CARTESIAN_POINT('Ctrl Pts',(163.916305873995,-3.724329161324,330.402467742298));
#23051=CARTESIAN_POINT('Ctrl Pts',(163.923704543749,-3.60196781977197,330.303346325195));
#23052=CARTESIAN_POINT('Ctrl Pts',(163.931103213504,-3.47558092415764,330.209059944536));
#23053=CARTESIAN_POINT('Ctrl Pts',(163.938501883259,-3.34559180536345,330.119944054175));
#23054=CARTESIAN_POINT('Ctrl Pts',(163.945899332463,-3.21562413073736,330.030842865168));
#23055=CARTESIAN_POINT('Ctrl Pts',(163.953296781667,-3.08205571985588,329.946910684414));
#23056=CARTESIAN_POINT('Ctrl Pts',(163.960694230871,-2.94534062713134,329.868440865325));
#23057=CARTESIAN_POINT('Ctrl Pts',(163.968091359334,-2.80863146213506,329.78997444855));
#23058=CARTESIAN_POINT('Ctrl Pts',(163.975488487798,-2.66877621025649,329.716970108311));
#23059=CARTESIAN_POINT('Ctrl Pts',(163.982885616261,-2.52625514223635,329.649676129539));
#23060=CARTESIAN_POINT('Ctrl Pts',(163.990283883698,-2.38371212952913,329.582371789174));
#23061=CARTESIAN_POINT('Ctrl Pts',(163.997682151135,-2.23850282088555,329.520779720343));
#23062=CARTESIAN_POINT('Ctrl Pts',(164.005080418571,-2.09112901432192,329.465100722871));
#23063=CARTESIAN_POINT('Ctrl Pts',(164.012481285097,-1.94370343379014,329.409402164782));
#23064=CARTESIAN_POINT('Ctrl Pts',(164.019882151623,-1.79411219026686,329.359620945821));
#23065=CARTESIAN_POINT('Ctrl Pts',(164.027283018149,-1.64287369468434,329.315908464335));
#23066=CARTESIAN_POINT('Ctrl Pts',(164.034692011533,-1.49146912477484,329.272147982366));
#23067=CARTESIAN_POINT('Ctrl Pts',(164.042101004918,-1.33841404920527,329.234469650033));
#23068=CARTESIAN_POINT('Ctrl Pts',(164.049509998303,-1.18423928171315,329.202974220676));
#23069=CARTESIAN_POINT('Ctrl Pts',(164.056923555883,-1.02996953724637,329.171459389048));
#23070=CARTESIAN_POINT('Ctrl Pts',(164.064337113463,-0.874579093892461,
329.146135109987));
#23071=CARTESIAN_POINT('Ctrl Pts',(164.071750671044,-0.718604892489981,
329.127050351741));
#23072=CARTESIAN_POINT('Ctrl Pts',(164.07917478318,-0.56240863325677,329.107938422847));
#23073=CARTESIAN_POINT('Ctrl Pts',(164.086598895317,-0.405627327088993,
329.095083786511));
#23074=CARTESIAN_POINT('Ctrl Pts',(164.094023007454,-0.248799751770714,
329.088483337923));
#23075=CARTESIAN_POINT('Ctrl Pts',(164.097880132609,-0.167321512411918,
329.085054139142));
#23076=CARTESIAN_POINT('Ctrl Pts',(164.101737257763,-0.0858307416424396,
329.083312225674));
#23077=CARTESIAN_POINT('Ctrl Pts',(164.105594382918,-0.0044024363394424,
329.083251637846));
#23078=CARTESIAN_POINT('Ctrl Pts',(164.113018360356,0.152326183331536,329.083135021805));
#23079=CARTESIAN_POINT('Ctrl Pts',(164.120442337794,0.30929587259952,329.089249901891));
#23080=CARTESIAN_POINT('Ctrl Pts',(164.127866315232,0.465970376285192,329.101627159044));
#23081=CARTESIAN_POINT('Ctrl Pts',(164.135281531259,0.622459980483371,329.113989809172));
#23082=CARTESIAN_POINT('Ctrl Pts',(164.142696747287,0.778654724088107,329.132600096257));
#23083=CARTESIAN_POINT('Ctrl Pts',(164.150111963315,0.934016813004763,329.157436936111));
#23084=CARTESIAN_POINT('Ctrl Pts',(164.157520044459,1.08922941330183,329.182249878082));
#23085=CARTESIAN_POINT('Ctrl Pts',(164.164928125603,1.24361058783445,329.213277387022));
#23086=CARTESIAN_POINT('Ctrl Pts',(164.172336206747,1.3966262404225,329.250446477589));
#23087=CARTESIAN_POINT('Ctrl Pts',(164.179738773921,1.54952800066658,329.287587902525));
#23088=CARTESIAN_POINT('Ctrl Pts',(164.187141341095,1.70106590162092,329.330861719264));
#23089=CARTESIAN_POINT('Ctrl Pts',(164.194543908269,1.85071474839632,329.380143642177));
#23090=CARTESIAN_POINT('Ctrl Pts',(164.201942578024,2.00028480570807,329.429399618372));
#23091=CARTESIAN_POINT('Ctrl Pts',(164.209341247779,2.14796743601218,329.484657284515));
#23092=CARTESIAN_POINT('Ctrl Pts',(164.216739917533,2.29325146037542,329.545742185963));
#23093=CARTESIAN_POINT('Ctrl Pts',(164.224137366737,2.43851151738538,329.606817010298));
#23094=CARTESIAN_POINT('Ctrl Pts',(164.231534815941,2.5813734100781,329.673717017532));
#23095=CARTESIAN_POINT('Ctrl Pts',(164.238932265145,2.72134473641413,329.746219133986));
#23096=CARTESIAN_POINT('Ctrl Pts',(164.246329393609,2.86130999383728,329.818718106875));
#23097=CARTESIAN_POINT('Ctrl Pts',(164.253726522072,2.99838460270778,329.89681853437));
#23098=CARTESIAN_POINT('Ctrl Pts',(164.261123650536,3.1320998728743,329.98025090778));
#23099=CARTESIAN_POINT('Ctrl Pts',(164.268521917972,3.26583573185466,330.063696127694));
#23100=CARTESIAN_POINT('Ctrl Pts',(164.275920185409,3.39621090555928,330.15247473064));
#23101=CARTESIAN_POINT('Ctrl Pts',(164.283318452846,3.52278498543111,330.24627340827));
#23102=CARTESIAN_POINT('Ctrl Pts',(164.290719319371,3.64940353210877,330.340105038362));
#23103=CARTESIAN_POINT('Ctrl Pts',(164.298120185897,3.77221802658342,330.438960032405));
#23104=CARTESIAN_POINT('Ctrl Pts',(164.305521052423,3.89082061285271,330.542484377919));
#23105=CARTESIAN_POINT('Ctrl Pts',(164.312930045808,4.00955343610021,330.646122403061));
#23106=CARTESIAN_POINT('Ctrl Pts',(164.320339039192,4.12406483328007,330.754439773787));
#23107=CARTESIAN_POINT('Ctrl Pts',(164.327748032577,4.23398282498811,330.867044640913));
#23108=CARTESIAN_POINT('Ctrl Pts',(164.335161590157,4.34396852997044,330.979718876522));
#23109=CARTESIAN_POINT('Ctrl Pts',(164.342575147738,4.44935494170331,331.096685594941));
#23110=CARTESIAN_POINT('Ctrl Pts',(164.349988705318,4.54981031224479,331.217519770694));
#23111=CARTESIAN_POINT('Ctrl Pts',(164.357412817455,4.65040869939692,331.338525976018));
#23112=CARTESIAN_POINT('Ctrl Pts',(164.364836929591,4.74606179820977,331.463410339836));
#23113=CARTESIAN_POINT('Ctrl Pts',(164.372261041728,4.83648065601138,331.591718112226));
#23114=CARTESIAN_POINT('Ctrl Pts',(164.376118166883,4.88345689296068,331.658379165736));
#23115=CARTESIAN_POINT('Ctrl Pts',(164.379975292037,4.92902103716036,331.725963844075));
#23116=CARTESIAN_POINT('Ctrl Pts',(164.383832417192,4.97313751511081,331.794405855649));
#23117=CARTESIAN_POINT('Ctrl Pts',(164.39125639463,5.05805042921793,331.926139187957));
#23118=CARTESIAN_POINT('Ctrl Pts',(164.398680372068,5.13785360187958,332.061447460951));
#23119=CARTESIAN_POINT('Ctrl Pts',(164.406104349506,5.21223086620783,332.199896437656));
#23120=CARTESIAN_POINT('Ctrl Pts',(164.413519565533,5.28652035417359,332.338182023739));
#23121=CARTESIAN_POINT('Ctrl Pts',(164.420934781561,5.35539650494734,332.479600610105));
#23122=CARTESIAN_POINT('Ctrl Pts',(164.428349997588,5.41858601743149,332.623688544362));
#23123=CARTESIAN_POINT('Ctrl Pts',(164.435758078733,5.48171472928466,332.767637837934));
#23124=CARTESIAN_POINT('Ctrl Pts',(164.443166159877,5.53916754700382,332.914251026621));
#23125=CARTESIAN_POINT('Ctrl Pts',(164.450574241021,5.59071681542903,333.063039480996));
#23126=CARTESIAN_POINT('Ctrl Pts',(164.457976808195,5.6422277147924,333.211717189408));
#23127=CARTESIAN_POINT('Ctrl Pts',(164.465379375369,5.6878436925393,333.362566588527));
#23128=CARTESIAN_POINT('Ctrl Pts',(164.472781942543,5.7273850500172,333.515078772682));
#23129=CARTESIAN_POINT('Ctrl Pts',(164.480180612297,5.76690558914336,333.667510659839));
#23130=CARTESIAN_POINT('Ctrl Pts',(164.487579282052,5.80035778409847,333.821603228166));
#23131=CARTESIAN_POINT('Ctrl Pts',(164.494977951807,5.82761170926055,333.976832208976));
#23132=CARTESIAN_POINT('Ctrl Pts',(164.502375401011,5.85486113837116,334.132035581823));
#23133=CARTESIAN_POINT('Ctrl Pts',(164.509772850215,5.87591426258902,334.288374627849));
#23134=CARTESIAN_POINT('Ctrl Pts',(164.517170299419,5.8906922023313,334.445314557706));
#23135=CARTESIAN_POINT('Ctrl Pts',(164.524567427882,5.90546950132787,334.602247682921));
#23136=CARTESIAN_POINT('Ctrl Pts',(164.531964556346,5.91397212184771,334.759781268597));
#23137=CARTESIAN_POINT('Ctrl Pts',(164.539361684809,5.91617306436292,334.917375336572));
#23138=CARTESIAN_POINT('Ctrl Pts',(164.546759952246,5.91837434576833,335.074993670098));
#23139=CARTESIAN_POINT('Ctrl Pts',(164.554158219683,5.91427201195984,335.232672131268));
#23140=CARTESIAN_POINT('Ctrl Pts',(164.561556487119,5.90389120027205,335.389870822004));
#23141=CARTESIAN_POINT('Ctrl Pts',(164.568957353645,5.89350674169596,335.547124738293));
#23142=CARTESIAN_POINT('Ctrl Pts',(164.576358220171,5.87683943828142,335.703898176403));
#23143=CARTESIAN_POINT('Ctrl Pts',(164.583759086696,5.85396627238938,335.859656585055));
#23144=CARTESIAN_POINT('Ctrl Pts',(164.591168080081,5.83106798957435,336.01558603133));
#23145=CARTESIAN_POINT('Ctrl Pts',(164.598577073466,5.8019502893581,336.170497852761));
#23146=CARTESIAN_POINT('Ctrl Pts',(164.605986066851,5.76674138667862,336.323867191854));
#23147=CARTESIAN_POINT('Ctrl Pts',(164.613399624431,5.7315107941005,336.477331011751));
#23148=CARTESIAN_POINT('Ctrl Pts',(164.620813182011,5.69018161966588,336.629250096583));
#23149=CARTESIAN_POINT('Ctrl Pts',(164.628226739592,5.64293174851916,336.779115466757));
#23150=CARTESIAN_POINT('Ctrl Pts',(164.635650851728,5.59561460853084,336.929194197721));
#23151=CARTESIAN_POINT('Ctrl Pts',(164.643074963865,5.54236006304602,337.077213024308));
#23152=CARTESIAN_POINT('Ctrl Pts',(164.650499076002,5.48339415210699,337.222682868773));
#23153=CARTESIAN_POINT('Ctrl Pts',(164.654356201156,5.4527589873675,337.298260309686));
#23154=CARTESIAN_POINT('Ctrl Pts',(164.658213326311,5.42058296239184,337.373150118072));
#23155=CARTESIAN_POINT('Ctrl Pts',(164.662070451466,5.38690257233349,337.447286505231));
#23156=CARTESIAN_POINT('Ctrl Pts',(164.669494428904,5.32207645291337,337.58998005121));
#23157=CARTESIAN_POINT('Ctrl Pts',(164.676918406342,5.25147891531012,337.730311312131));
#23158=CARTESIAN_POINT('Ctrl Pts',(164.68434238378,5.17530402261369,337.86777942597));
#23159=CARTESIAN_POINT('Ctrl Pts',(164.691757599807,5.09921902775163,338.005085306752));
#23160=CARTESIAN_POINT('Ctrl Pts',(164.699172815835,5.01756995873937,338.139534443025));
#23161=CARTESIAN_POINT('Ctrl Pts',(164.706588031863,4.93059881185969,338.270646101153));
#23162=CARTESIAN_POINT('Ctrl Pts',(164.713996113007,4.84371134817957,338.401631604304));
#23163=CARTESIAN_POINT('Ctrl Pts',(164.721404194151,4.75151220626657,338.529285713488));
#23164=CARTESIAN_POINT('Ctrl Pts',(164.728812275295,4.65428908776097,338.653152563205));
#23165=CARTESIAN_POINT('Ctrl Pts',(164.736214842469,4.55713833419801,338.776927216563));
#23166=CARTESIAN_POINT('Ctrl Pts',(164.743617409643,4.45497127925033,338.896919931025));
#23167=CARTESIAN_POINT('Ctrl Pts',(164.751019976817,4.34811862730315,339.0127041961));
#23168=CARTESIAN_POINT('Ctrl Pts',(164.758418646572,4.24132223281057,339.128427501265));
#23169=CARTESIAN_POINT('Ctrl Pts',(164.765817316326,4.1298454068607,339.239946496225));
#23170=CARTESIAN_POINT('Ctrl Pts',(164.773215986081,4.0140587079684,339.346868211883));
#23171=CARTESIAN_POINT('Ctrl Pts',(164.780613435285,3.89829111028591,339.453772288779));
#23172=CARTESIAN_POINT('Ctrl Pts',(164.788010884489,3.77821532467789,339.55608033862));
#23173=CARTESIAN_POINT('Ctrl Pts',(164.795408333693,3.65423838064705,339.653436624679));
#23174=CARTESIAN_POINT('Ctrl Pts',(164.802805462157,3.53026681204053,339.75078868954));
#23175=CARTESIAN_POINT('Ctrl Pts',(164.81020259062,3.4023947148572,339.843189187015));
#23176=CARTESIAN_POINT('Ctrl Pts',(164.817599719084,3.27106155726081,339.930323199458));
#23177=CARTESIAN_POINT('Ctrl Pts',(164.82499798652,3.13970817763637,340.017470628363));
#23178=CARTESIAN_POINT('Ctrl Pts',(164.832396253957,3.00489298750044,340.099349751271));
#23179=CARTESIAN_POINT('Ctrl Pts',(164.839794521393,2.86708360191832,340.175689536874));
#23180=CARTESIAN_POINT('Ctrl Pts',(164.847195387919,2.72922580245032,340.252056141447));
#23181=CARTESIAN_POINT('Ctrl Pts',(164.854596254445,2.58837203948197,340.322879353443));
#23182=CARTESIAN_POINT('Ctrl Pts',(164.861997120971,2.44501348816116,340.387934632604));
#23183=CARTESIAN_POINT('Ctrl Pts',(164.869406114355,2.3014975154447,340.453061348681));
#23184=CARTESIAN_POINT('Ctrl Pts',(164.87681510774,2.15547160154408,340.512407328785));
#23185=CARTESIAN_POINT('Ctrl Pts',(164.884224101125,2.00744649478331,340.565796361086));
#23186=CARTESIAN_POINT('Ctrl Pts',(164.891637658705,1.85933019945115,340.619218282873));
#23187=CARTESIAN_POINT('Ctrl Pts',(164.899051216285,1.70921261221028,340.66667583229));
#23188=CARTESIAN_POINT('Ctrl Pts',(164.906464773866,1.55761800871999,340.708043158685));
#23189=CARTESIAN_POINT('Ctrl Pts',(164.913888886002,1.40580758255848,340.749469379042));
#23190=CARTESIAN_POINT('Ctrl Pts',(164.921312998139,1.2525163031314,340.784787975993));
#23191=CARTESIAN_POINT('Ctrl Pts',(164.928737110276,1.09827776958484,340.8139243634));
#23192=CARTESIAN_POINT('Ctrl Pts',(164.93259423543,1.01814464166175,340.829061889708));
#23193=CARTESIAN_POINT('Ctrl Pts',(164.936451360585,0.937755910711731,340.842531556355));
#23194=CARTESIAN_POINT('Ctrl Pts',(164.94030848574,0.857186649477655,340.854328450852));
#23195=CARTESIAN_POINT('Ctrl Pts',(164.947732463178,0.702111469489997,340.877034449511));
#23196=CARTESIAN_POINT('Ctrl Pts',(164.955156440616,0.545899539862234,340.893608771498));
#23197=CARTESIAN_POINT('Ctrl Pts',(164.962580418054,0.38907706482888,340.903943563426));
#23198=CARTESIAN_POINT('Ctrl Pts',(164.969995634081,0.232439663911139,340.914266158745));
#23199=CARTESIAN_POINT('Ctrl Pts',(164.977410850109,0.0751935206070489,
340.918363857034));
#23200=CARTESIAN_POINT('Ctrl Pts',(164.984826066137,-0.0821261478370629,
340.916180005573));
#23201=CARTESIAN_POINT('Ctrl Pts',(164.992234147281,-0.239294444088226,
340.913998255403));
#23202=CARTESIAN_POINT('Ctrl Pts',(164.999642228425,-0.396535753957013,
340.905546993257));
#23203=CARTESIAN_POINT('Ctrl Pts',(165.007050309569,-0.553311038551743,
340.890821458601));
#23204=CARTESIAN_POINT('Ctrl Pts',(165.014452876743,-0.709969632438892,
340.87610688443));
#23205=CARTESIAN_POINT('Ctrl Pts',(165.021855443917,-0.866162521738701,
340.855127371262));
#23206=CARTESIAN_POINT('Ctrl Pts',(165.029258011091,-1.02135208156133,340.82793020617));
#23207=CARTESIAN_POINT('Ctrl Pts',(165.036656680846,-1.1764599347584,340.800747360267));
#23208=CARTESIAN_POINT('Ctrl Pts',(165.0440553506,-1.33056514383375,340.767353446203));
#23209=CARTESIAN_POINT('Ctrl Pts',(165.051454020355,-1.48313672221534,340.727847416414));
#23210=CARTESIAN_POINT('Ctrl Pts',(165.058851469559,-1.63568313102466,340.688347903892));
#23211=CARTESIAN_POINT('Ctrl Pts',(165.066248918763,-1.78669605032176,340.642738370273));
#23212=CARTESIAN_POINT('Ctrl Pts',(165.073646367967,-1.9356560664853,340.591168585795));
#23213=CARTESIAN_POINT('Ctrl Pts',(165.08104349643,-2.08460962400221,340.539601037293));
#23214=CARTESIAN_POINT('Ctrl Pts',(165.088440624894,-2.23151010269279,340.482073873863));
#23215=CARTESIAN_POINT('Ctrl Pts',(165.095837753357,-2.37585486014896,340.418786233651));
#23216=CARTESIAN_POINT('Ctrl Pts',(165.103236020794,-2.52022184309527,340.355488848722));
#23217=CARTESIAN_POINT('Ctrl Pts',(165.110634288231,-2.66203197944046,340.286429370809));
#23218=CARTESIAN_POINT('Ctrl Pts',(165.118032555667,-2.80080429983198,340.211854356805));
#23219=CARTESIAN_POINT('Ctrl Pts',(165.125433422193,-2.93962537239833,340.137253143813));
#23220=CARTESIAN_POINT('Ctrl Pts',(165.132834288719,-3.07540617564299,340.057132713396));
#23221=CARTESIAN_POINT('Ctrl Pts',(165.140235155245,-3.20769208581463,339.971784593594));
#23222=CARTESIAN_POINT('Ctrl Pts',(165.147644148629,-3.3401232585626,339.886342753398));
#23223=CARTESIAN_POINT('Ctrl Pts',(165.155053142014,-3.46905156029963,339.795661962178));
#23224=CARTESIAN_POINT('Ctrl Pts',(165.162462135399,-3.59405241551403,339.700076360767));
#23225=CARTESIAN_POINT('Ctrl Pts',(165.169875692979,-3.71913027556667,339.604431875328));
#23226=CARTESIAN_POINT('Ctrl Pts',(165.177289250559,-3.84027558153471,339.503876796702));
#23227=CARTESIAN_POINT('Ctrl Pts',(165.184702808139,-3.95709878727818,339.398783894467));
#23228=CARTESIAN_POINT('Ctrl Pts',(165.192126920276,-4.07408831224296,339.293541373245));
#23229=CARTESIAN_POINT('Ctrl Pts',(165.199551032413,-4.18674318105786,339.183748385439));
#23230=CARTESIAN_POINT('Ctrl Pts',(165.20697514455,-4.29471191153351,339.069813283117));
#23231=CARTESIAN_POINT('Ctrl Pts',(165.210832269704,-4.35080601390779,339.010619410358));
#23232=CARTESIAN_POINT('Ctrl Pts',(165.214689394859,-4.40563589897465,338.950308020996));
#23233=CARTESIAN_POINT('Ctrl Pts',(165.218546520014,-4.4591568095499,338.888939586873));
#23234=CARTESIAN_POINT('Ctrl Pts',(165.225910699378,-4.56134109692491,338.77177249011));
#23235=CARTESIAN_POINT('Ctrl Pts',(165.233274878743,-4.65907261310312,338.650382016011));
#23236=CARTESIAN_POINT('Ctrl Pts',(165.240639058108,-4.75197758073249,338.52514391688));
#23237=CARTESIAN_POINT('Ctrl Pts',(165.248041664866,-4.84536734042338,338.399252306556));
#23238=CARTESIAN_POINT('Ctrl Pts',(165.255444271623,-4.93387972720829,338.269473038242));
#23239=CARTESIAN_POINT('Ctrl Pts',(165.262846878381,-5.01717244490983,338.136225632912));
#23240=CARTESIAN_POINT('Ctrl Pts',(165.270193032476,-5.09982996802607,338.003994379207));
#23241=CARTESIAN_POINT('Ctrl Pts',(165.277539186571,-5.1773469283478,337.868348013314));
#23242=CARTESIAN_POINT('Ctrl Pts',(165.284885340665,-5.24942928621526,337.7297294246));
#23243=CARTESIAN_POINT('Ctrl Pts',(165.292226440061,-5.32146204607451,337.591206215756));
#23244=CARTESIAN_POINT('Ctrl Pts',(165.299567539457,-5.38806746989197,337.449715189005));
#23245=CARTESIAN_POINT('Ctrl Pts',(165.306908638853,-5.44899585100362,337.305726518528));
#23246=CARTESIAN_POINT('Ctrl Pts',(165.314246194793,-5.50989482275996,337.161807349553));
#23247=CARTESIAN_POINT('Ctrl Pts',(165.321583750734,-5.56512205836557,337.015393285453));
#23248=CARTESIAN_POINT('Ctrl Pts',(165.328921306674,-5.61447478306401,336.866977094889));
#23249=CARTESIAN_POINT('Ctrl Pts',(165.336369666142,-5.66457277717538,336.716319689722));
#23250=CARTESIAN_POINT('Ctrl Pts',(165.343818025611,-5.70861722990409,336.563599560885));
#23251=CARTESIAN_POINT('Ctrl Pts',(165.351266385079,-5.74644758458795,336.409351169895));
#23252=CARTESIAN_POINT('Ctrl Pts',(165.358602757873,-5.78370915689436,336.257421915673));
#23253=CARTESIAN_POINT('Ctrl Pts',(165.365939130667,-5.81494212088197,336.104010418292));
#23254=CARTESIAN_POINT('Ctrl Pts',(165.373275503461,-5.84004403237057,335.94964006996));
#23255=CARTESIAN_POINT('Ctrl Pts',(165.380779856267,-5.86572069919064,335.791735123046));
#23256=CARTESIAN_POINT('Ctrl Pts',(165.388284209072,-5.88498207564688,335.632827293128));
#23257=CARTESIAN_POINT('Ctrl Pts',(165.395788561878,-5.89777443037654,335.473484245669));
#23258=CARTESIAN_POINT('Ctrl Pts',(165.403292914683,-5.9105667851062,335.31414119821));
#23259=CARTESIAN_POINT('Ctrl Pts',(165.410797267489,-5.91689011634911,335.154363357795));
#23260=CARTESIAN_POINT('Ctrl Pts',(165.418301620294,-5.9167476438022,334.994719653312));
#23261=CARTESIAN_POINT('',(167.168301620294,-5.92209282452846,335.000276467281));
#23262=CARTESIAN_POINT('Ctrl Pts',(165.418302861901,-5.9138621938537,334.994695827962));
#23263=CARTESIAN_POINT('Ctrl Pts',(165.44446342603,-5.91863216628149,334.438436333665));
#23264=CARTESIAN_POINT('Ctrl Pts',(165.563370001584,-5.59117675901454,331.91560276841));
#23265=CARTESIAN_POINT('Ctrl Pts',(165.775022588561,-2.00088777716957,328.295593163865));
#23266=CARTESIAN_POINT('Ctrl Pts',(166.053260622836,4.55508355360873,329.689271543295));
#23267=CARTESIAN_POINT('Ctrl Pts',(166.331498657109,6.93092194016336,335.956527041217));
#23268=CARTESIAN_POINT('Ctrl Pts',(166.609736691382,2.94635556247053,341.345991791731));
#23269=CARTESIAN_POINT('Ctrl Pts',(166.887974725657,-3.74203782676519,340.911833541658));
#23270=CARTESIAN_POINT('Ctrl Pts',(167.074163035294,-5.91976887378537,336.990930151837));
#23271=CARTESIAN_POINT('Ctrl Pts',(167.167605333506,-5.92649389691024,335.015000414505));
#23272=CARTESIAN_POINT('Ctrl Pts',(167.168301620294,-5.92648390138188,335.000276672274));
#23273=CARTESIAN_POINT('',(168.91830160198,-5.91441582040877,335.005131115878));
#23274=CARTESIAN_POINT('Ctrl Pts',(167.168301620294,-5.91674999355252,335.000276217856));
#23275=CARTESIAN_POINT('Ctrl Pts',(167.175715681463,-5.9167573005817,334.843755326903));
#23276=CARTESIAN_POINT('Ctrl Pts',(167.183129742633,-5.91054944576592,334.686995018447));
#23277=CARTESIAN_POINT('Ctrl Pts',(167.190543803802,-5.89809535193679,334.530530318379));
#23278=CARTESIAN_POINT('Ctrl Pts',(167.197949113985,-5.88565595796128,334.374250297197));
#23279=CARTESIAN_POINT('Ctrl Pts',(167.205354424167,-5.86698502891278,334.218265559408));
#23280=CARTESIAN_POINT('Ctrl Pts',(167.212759734349,-5.84210345250691,334.063112700104));
#23281=CARTESIAN_POINT('Ctrl Pts',(167.22015792973,-5.8172457815783,333.908108907044));
#23282=CARTESIAN_POINT('Ctrl Pts',(167.227556125111,-5.78618940081505,333.753935768526));
#23283=CARTESIAN_POINT('Ctrl Pts',(167.234954320492,-5.7490071008753,333.601126197048));
#23284=CARTESIAN_POINT('Ctrl Pts',(167.242347031577,-5.71185236424428,333.448429903592));
#23285=CARTESIAN_POINT('Ctrl Pts',(167.249739742662,-5.6685808382736,333.297095526752));
#23286=CARTESIAN_POINT('Ctrl Pts',(167.257132453747,-5.61931661459518,333.147647078056));
#23287=CARTESIAN_POINT('Ctrl Pts',(167.264521306644,-5.57007810146327,332.998276625135));
#23288=CARTESIAN_POINT('Ctrl Pts',(167.27191015954,-5.51485323596182,332.850790494876));
#23289=CARTESIAN_POINT('Ctrl Pts',(167.279299012437,-5.45381627519081,332.705698668665));
#23290=CARTESIAN_POINT('Ctrl Pts',(167.286686699553,-5.39278894456899,332.560629734419));
#23291=CARTESIAN_POINT('Ctrl Pts',(167.294074386668,-5.32595148320592,332.417954699395));
#23292=CARTESIAN_POINT('Ctrl Pts',(167.301462073783,-5.2535267570549,332.278164741317));
#23293=CARTESIAN_POINT('Ctrl Pts',(167.308849493468,-5.18110465263808,332.138379843557));
#23294=CARTESIAN_POINT('Ctrl Pts',(167.316236913154,-5.10309585771362,332.001480147508));
#23295=CARTESIAN_POINT('Ctrl Pts',(167.323624332839,-5.01976965201283,331.867933078105));
#23296=CARTESIAN_POINT('Ctrl Pts',(167.331012953445,-4.93642990055476,331.73436429889));
#23297=CARTESIAN_POINT('Ctrl Pts',(167.338401574051,-4.84777121546881,331.604149549024));
#23298=CARTESIAN_POINT('Ctrl Pts',(167.345790194658,-4.75410664191021,331.477727920809));
#23299=CARTESIAN_POINT('Ctrl Pts',(167.353181484987,-4.6604082246238,331.351260612793));
#23300=CARTESIAN_POINT('Ctrl Pts',(167.360572775316,-4.56170054051903,331.228589455613));
#23301=CARTESIAN_POINT('Ctrl Pts',(167.367964065645,-4.45833728934662,331.110120930296));
#23302=CARTESIAN_POINT('Ctrl Pts',(167.375363486064,-4.35486034321604,330.991522094894));
#23303=CARTESIAN_POINT('Ctrl Pts',(167.382762906482,-4.24671785033054,330.877135404564));
#23304=CARTESIAN_POINT('Ctrl Pts',(167.390162326901,-4.13430126835267,330.767331387293));
#23305=CARTESIAN_POINT('Ctrl Pts',(167.397566391386,-4.0218141308228,330.657458454182));
#23306=CARTESIAN_POINT('Ctrl Pts',(167.404970455872,-3.90504783664909,330.552174174841));
#23307=CARTESIAN_POINT('Ctrl Pts',(167.412374520358,-3.78442693156098,330.451808781265));
#23308=CARTESIAN_POINT('Ctrl Pts',(167.419788972678,-3.66363679646266,330.351302575974));
#23309=CARTESIAN_POINT('Ctrl Pts',(167.427203424997,-3.53898154728273,330.255729264417));
#23310=CARTESIAN_POINT('Ctrl Pts',(167.434617877317,-3.41091529904489,330.165376189894));
#23311=CARTESIAN_POINT('Ctrl Pts',(167.43789551628,-3.35430222677227,330.125434634579));
#23312=CARTESIAN_POINT('Ctrl Pts',(167.441173155242,-3.29702291921798,330.086512609086));
#23313=CARTESIAN_POINT('Ctrl Pts',(167.444450794205,-3.23911807713838,330.048632043076));
#23314=CARTESIAN_POINT('Ctrl Pts',(167.451874771643,-3.10796139818704,329.962831114237));
#23315=CARTESIAN_POINT('Ctrl Pts',(167.459298749081,-2.97319534018959,329.882115658969));
#23316=CARTESIAN_POINT('Ctrl Pts',(167.466722726519,-2.83525199427725,329.806804770525));
#23317=CARTESIAN_POINT('Ctrl Pts',(167.474137942547,-2.69747144226737,329.73158276026));
#23318=CARTESIAN_POINT('Ctrl Pts',(167.481553158574,-2.55652139052194,329.661752798007));
#23319=CARTESIAN_POINT('Ctrl Pts',(167.488968374602,-2.41286363450969,329.597591310928));
#23320=CARTESIAN_POINT('Ctrl Pts',(167.496376455746,-2.26934410526747,329.533491559709));
#23321=CARTESIAN_POINT('Ctrl Pts',(167.50378453689,-2.12312239699419,329.475049576592));
#23322=CARTESIAN_POINT('Ctrl Pts',(167.511192618034,-1.97468558999428,329.422496312581));
#23323=CARTESIAN_POINT('Ctrl Pts',(167.518595185208,-1.82635926722023,329.369982164924));
#23324=CARTESIAN_POINT('Ctrl Pts',(167.525997752382,-1.67582147890356,329.323348133044));
#23325=CARTESIAN_POINT('Ctrl Pts',(167.533400319556,-1.52357990511136,329.282777349513));
#23326=CARTESIAN_POINT('Ctrl Pts',(167.540798989311,-1.37141848584261,329.242227926322));
#23327=CARTESIAN_POINT('Ctrl Pts',(167.548197659066,-1.2175554273154,329.207735489739));
#23328=CARTESIAN_POINT('Ctrl Pts',(167.55559632882,-1.06251410851324,329.179433504227));
#23329=CARTESIAN_POINT('Ctrl Pts',(167.562993778024,-0.907498366714359,
329.151136187665));
#23330=CARTESIAN_POINT('Ctrl Pts',(167.570391227228,-0.751305117202117,
329.129027362314));
#23331=CARTESIAN_POINT('Ctrl Pts',(167.577788676432,-0.59446860423178,329.113189518841));
#23332=CARTESIAN_POINT('Ctrl Pts',(167.585185804896,-0.437638891419135,
329.097352362069));
#23333=CARTESIAN_POINT('Ctrl Pts',(167.592582933359,-0.280166341927268,
329.087785684047));
#23334=CARTESIAN_POINT('Ctrl Pts',(167.599980061823,-0.122590739196191,
329.084520131624));
#23335=CARTESIAN_POINT('Ctrl Pts',(167.607378329259,0.0350091262437524,
329.081254076387));
#23336=CARTESIAN_POINT('Ctrl Pts',(167.614776596696,0.192711703363562,329.08429108631));
#23337=CARTESIAN_POINT('Ctrl Pts',(167.622174864132,0.349976936586156,329.093609672028));
#23338=CARTESIAN_POINT('Ctrl Pts',(167.629575730658,0.507297418738823,329.102931531463));
#23339=CARTESIAN_POINT('Ctrl Pts',(167.636976597184,0.664179878767207,329.118539338334));
#23340=CARTESIAN_POINT('Ctrl Pts',(167.64437746371,0.820089257519572,329.140359723311));
#23341=CARTESIAN_POINT('Ctrl Pts',(167.651786457094,0.976169839675887,329.162204069156));
#23342=CARTESIAN_POINT('Ctrl Pts',(167.659195450479,1.13127483680275,329.190274565255));
#23343=CARTESIAN_POINT('Ctrl Pts',(167.666604443864,1.28487853720021,329.224446545383));
#23344=CARTESIAN_POINT('Ctrl Pts',(167.674018001444,1.43857686277542,329.258639576628));
#23345=CARTESIAN_POINT('Ctrl Pts',(167.681431559024,1.59077168880065,329.298941486346));
#23346=CARTESIAN_POINT('Ctrl Pts',(167.688845116605,1.74095284555439,329.345177831969));
#23347=CARTESIAN_POINT('Ctrl Pts',(167.696269228741,1.8913478126791,329.391480003495));
#23348=CARTESIAN_POINT('Ctrl Pts',(167.703693340878,2.03972303383535,329.443733361146));
#23349=CARTESIAN_POINT('Ctrl Pts',(167.711117453015,2.1855879153784,329.501715174106));
#23350=CARTESIAN_POINT('Ctrl Pts',(167.714974578169,2.26137059395679,329.531839060326));
#23351=CARTESIAN_POINT('Ctrl Pts',(167.718831703324,2.33647606530862,329.563508417066));
#23352=CARTESIAN_POINT('Ctrl Pts',(167.722688828479,2.41083829568462,329.596687194456));
#23353=CARTESIAN_POINT('Ctrl Pts',(167.730112805917,2.55396653197773,329.66054783804));
#23354=CARTESIAN_POINT('Ctrl Pts',(167.737536783355,2.69477152715902,329.73019572702));
#23355=CARTESIAN_POINT('Ctrl Pts',(167.744960760793,2.83275111960009,329.805440186416));
#23356=CARTESIAN_POINT('Ctrl Pts',(167.75237597682,2.97056787536166,329.880595846028));
#23357=CARTESIAN_POINT('Ctrl Pts',(167.759791192848,3.10556554108869,329.96133475216));
#23358=CARTESIAN_POINT('Ctrl Pts',(167.767206408876,3.23726175925666,330.047418161751));
#23359=CARTESIAN_POINT('Ctrl Pts',(167.77461449002,3.36883125998668,330.133418742318));
#23360=CARTESIAN_POINT('Ctrl Pts',(167.782022571164,3.49710532694165,330.224753385844));
#23361=CARTESIAN_POINT('Ctrl Pts',(167.789430652308,3.62162616139335,330.321137476949));
#23362=CARTESIAN_POINT('Ctrl Pts',(167.796833219482,3.74605431271341,330.417449827614));
#23363=CARTESIAN_POINT('Ctrl Pts',(167.804235786656,3.86673450012886,330.518803914882));
#23364=CARTESIAN_POINT('Ctrl Pts',(167.81163835383,3.98323798873801,330.624871923295));
#23365=CARTESIAN_POINT('Ctrl Pts',(167.819037023585,4.09968013877036,330.730884087366));
#23366=CARTESIAN_POINT('Ctrl Pts',(167.826435693339,4.2119496941873,330.841604979195));
#23367=CARTESIAN_POINT('Ctrl Pts',(167.833834363094,4.31965119147316,330.95666670351));
#23368=CARTESIAN_POINT('Ctrl Pts',(167.841231812298,4.42733492135617,331.071709446213));
#23369=CARTESIAN_POINT('Ctrl Pts',(167.848629261502,4.53045183394266,331.191091327964));
#23370=CARTESIAN_POINT('Ctrl Pts',(167.856026710706,4.62864345085063,331.314407731802));
#23371=CARTESIAN_POINT('Ctrl Pts',(167.86342383917,4.72683081034106,331.437718788857));
#23372=CARTESIAN_POINT('Ctrl Pts',(167.870820967633,4.8200930662888,331.56496373684));
#23373=CARTESIAN_POINT('Ctrl Pts',(167.878218096097,4.90811233931278,331.695705245111));
#23374=CARTESIAN_POINT('Ctrl Pts',(167.885616363533,4.99614516510755,331.826466884311));
#23375=CARTESIAN_POINT('Ctrl Pts',(167.89301463097,5.07893319212297,331.960725846181));
#23376=CARTESIAN_POINT('Ctrl Pts',(167.900412898406,5.15620223616344,332.098016357337));
#23377=CARTESIAN_POINT('Ctrl Pts',(167.907813764932,5.2334984256317,332.235355100094));
#23378=CARTESIAN_POINT('Ctrl Pts',(167.915214631458,5.30527158889137,332.375727187546));
#23379=CARTESIAN_POINT('Ctrl Pts',(167.922615497984,5.3712938725684,332.518642972684));
#23380=CARTESIAN_POINT('Ctrl Pts',(167.930024491368,5.437388655025,332.661715693018));
#23381=CARTESIAN_POINT('Ctrl Pts',(167.937433484753,5.49771978986544,332.807337350247));
#23382=CARTESIAN_POINT('Ctrl Pts',(167.944842478138,5.55210761881268,332.954998398137));
#23383=CARTESIAN_POINT('Ctrl Pts',(167.952256035718,5.60652895253851,333.102750410326));
#23384=CARTESIAN_POINT('Ctrl Pts',(167.959669593299,5.65499957015316,333.252543962336));
#23385=CARTESIAN_POINT('Ctrl Pts',(167.967083150879,5.69739008202169,333.403855640683));
#23386=CARTESIAN_POINT('Ctrl Pts',(167.974507263016,5.73984094454449,333.555382738904));
#23387=CARTESIAN_POINT('Ctrl Pts',(167.981931375152,5.77619432725514,333.708431917943));
#23388=CARTESIAN_POINT('Ctrl Pts',(167.989355487289,5.80637204087687,333.862470094713));
#23389=CARTESIAN_POINT('Ctrl Pts',(167.993212612444,5.82205057807774,333.942499129221));
#23390=CARTESIAN_POINT('Ctrl Pts',(167.997069737598,5.83606302045804,334.022795028504));
#23391=CARTESIAN_POINT('Ctrl Pts',(168.000926862753,5.84840394847278,334.103282754717));
#23392=CARTESIAN_POINT('Ctrl Pts',(168.008350840191,5.8721570722303,334.258201000689));
#23393=CARTESIAN_POINT('Ctrl Pts',(168.015774817629,5.8897863387954,334.414297394202));
#23394=CARTESIAN_POINT('Ctrl Pts',(168.023198795067,5.90118034235701,334.571046471656));
#23395=CARTESIAN_POINT('Ctrl Pts',(168.030614011094,5.9125608992801,334.727610561614));
#23396=CARTESIAN_POINT('Ctrl Pts',(168.038029227122,5.91772081371359,334.884825433678));
#23397=CARTESIAN_POINT('Ctrl Pts',(168.04544444315,5.91659981845783,335.042156265546));
#23398=CARTESIAN_POINT('Ctrl Pts',(168.052852524294,5.91547990181807,335.199335714479));
#23399=CARTESIAN_POINT('Ctrl Pts',(168.060260605438,5.90809110953202,335.35663053038));
#23400=CARTESIAN_POINT('Ctrl Pts',(168.067668686582,5.89442503958346,335.51350171882));
#23401=CARTESIAN_POINT('Ctrl Pts',(168.075071253756,5.88076914154034,335.67025614517));
#23402=CARTESIAN_POINT('Ctrl Pts',(168.08247382093,5.8608453013008,335.826587201684));
#23403=CARTESIAN_POINT('Ctrl Pts',(168.089876388104,5.8346971728197,335.981956956282));
#23404=CARTESIAN_POINT('Ctrl Pts',(168.097275057859,5.80856281121377,336.137244909384));
#23405=CARTESIAN_POINT('Ctrl Pts',(168.104673727613,5.7762107496097,336.291572201433));
#23406=CARTESIAN_POINT('Ctrl Pts',(168.112072397368,5.73773635099095,336.444407189478));
#23407=CARTESIAN_POINT('Ctrl Pts',(168.119469846572,5.69926829945352,336.597216964496));
#23408=CARTESIAN_POINT('Ctrl Pts',(168.126867295776,5.65468000643663,336.748534562539));
#23409=CARTESIAN_POINT('Ctrl Pts',(168.13426474498,5.60411772975157,336.897839570033));
#23410=CARTESIAN_POINT('Ctrl Pts',(168.141661873444,5.55355764535874,337.047138103923));
#23411=CARTESIAN_POINT('Ctrl Pts',(168.149059001907,5.49702421202805,337.19442386728));
#23412=CARTESIAN_POINT('Ctrl Pts',(168.15645613037,5.43471316765349,337.339192883846));
#23413=CARTESIAN_POINT('Ctrl Pts',(168.163854397807,5.37239252893368,337.483984191226));
#23414=CARTESIAN_POINT('Ctrl Pts',(168.171252665244,5.30429265540206,337.626257637394));
#23415=CARTESIAN_POINT('Ctrl Pts',(168.17865093268,5.23065684903385,337.765530598304));
#23416=CARTESIAN_POINT('Ctrl Pts',(168.186051799206,5.15699517363221,337.904852487271));
#23417=CARTESIAN_POINT('Ctrl Pts',(168.193452665732,5.07779386756958,338.041171462538));
#23418=CARTESIAN_POINT('Ctrl Pts',(168.200853532257,4.99334138092783,338.17403094125));
#23419=CARTESIAN_POINT('Ctrl Pts',(168.208262525642,4.90879615738172,338.307036312372));
#23420=CARTESIAN_POINT('Ctrl Pts',(168.215671519027,4.81898843797882,338.436574285263));
#23421=CARTESIAN_POINT('Ctrl Pts',(168.223080512412,4.72424948761407,338.56221803674));
#23422=CARTESIAN_POINT('Ctrl Pts',(168.230494069992,4.62945217478809,338.687939189103));
#23423=CARTESIAN_POINT('Ctrl Pts',(168.237907627572,4.52971781363256,338.809761051675));
#23424=CARTESIAN_POINT('Ctrl Pts',(168.245321185152,4.42541653355728,338.927291568883));
#23425=CARTESIAN_POINT('Ctrl Pts',(168.252745297289,4.32096676151517,339.044989412298));
#23426=CARTESIAN_POINT('Ctrl Pts',(168.260169409426,4.21193734304222,339.158383440123));
#23427=CARTESIAN_POINT('Ctrl Pts',(168.267593521562,4.09873424637482,339.267119419479));
#23428=CARTESIAN_POINT('Ctrl Pts',(168.271450646717,4.03992068002348,339.323612138538));
#23429=CARTESIAN_POINT('Ctrl Pts',(168.275307771872,3.97998108188275,339.378848218759));
#23430=CARTESIAN_POINT('Ctrl Pts',(168.279164897027,3.91897562004839,339.43278249545));
#23431=CARTESIAN_POINT('Ctrl Pts',(168.286588874465,3.80155574019379,339.536592156071));
#23432=CARTESIAN_POINT('Ctrl Pts',(168.294012851903,3.67983116042366,339.635889697768));
#23433=CARTESIAN_POINT('Ctrl Pts',(168.301436829341,3.55418346621271,339.730297078514));
#23434=CARTESIAN_POINT('Ctrl Pts',(168.308852045368,3.42868405518537,339.824593044347));
#23435=CARTESIAN_POINT('Ctrl Pts',(168.316267261396,3.29927104100951,339.914010114737));
#23436=CARTESIAN_POINT('Ctrl Pts',(168.323682477424,3.16636155312993,339.998208186677));
#23437=CARTESIAN_POINT('Ctrl Pts',(168.331090558568,3.03357995009088,340.082325243654));
#23438=CARTESIAN_POINT('Ctrl Pts',(168.338498639712,2.89730888418641,340.161233101047));
#23439=CARTESIAN_POINT('Ctrl Pts',(168.345906720856,2.75799706051858,340.234633012607));
#23440=CARTESIAN_POINT('Ctrl Pts',(168.35330928803,2.61878892918522,340.307978291271));
#23441=CARTESIAN_POINT('Ctrl Pts',(168.360711855204,2.47654487540259,340.375823613911));
#23442=CARTESIAN_POINT('Ctrl Pts',(168.368114422378,2.33174088139209,340.437914584153));
#23443=CARTESIAN_POINT('Ctrl Pts',(168.375513092133,2.18701312605077,340.499972863771));
#23444=CARTESIAN_POINT('Ctrl Pts',(168.382911761887,2.03972845684378,340.556282677993));
#23445=CARTESIAN_POINT('Ctrl Pts',(168.390310431642,1.89038555005136,340.60663651708));
#23446=CARTESIAN_POINT('Ctrl Pts',(168.397707880846,1.74106728020185,340.656982049348));
#23447=CARTESIAN_POINT('Ctrl Pts',(168.40510533005,1.589691799961,340.701373437403));
#23448=CARTESIAN_POINT('Ctrl Pts',(168.412502779254,1.43677588469872,340.739652046914));
#23449=CARTESIAN_POINT('Ctrl Pts',(168.419899907718,1.28386659960428,340.777928996732));
#23450=CARTESIAN_POINT('Ctrl Pts',(168.427297036181,1.12941737433057,340.810093604364));
#23451=CARTESIAN_POINT('Ctrl Pts',(168.434694164645,0.97395793827043,340.83603773951));
#23452=CARTESIAN_POINT('Ctrl Pts',(168.442092432081,0.818474565337374,340.861985869405));
#23453=CARTESIAN_POINT('Ctrl Pts',(168.449490699518,0.661981040045436,340.881711558275));
#23454=CARTESIAN_POINT('Ctrl Pts',(168.456888966955,0.505014875909126,340.895158228378));
#23455=CARTESIAN_POINT('Ctrl Pts',(168.46428983348,0.347993567909082,340.908609622438));
#23456=CARTESIAN_POINT('Ctrl Pts',(168.471690700006,0.190499662088425,340.915777573982));
#23457=CARTESIAN_POINT('Ctrl Pts',(168.479091566532,0.0330732056023354,
340.916657563656));
#23458=CARTESIAN_POINT('Ctrl Pts',(168.486500559917,-0.124526120183621,
340.917538519643));
#23459=CARTESIAN_POINT('Ctrl Pts',(168.493909553301,-0.282057475293545,
340.912117722452));
#23460=CARTESIAN_POINT('Ctrl Pts',(168.501318546686,-0.438982668565141,
340.900442761285));
#23461=CARTESIAN_POINT('Ctrl Pts',(168.508732104266,-0.596004533168329,
340.888760607939));
#23462=CARTESIAN_POINT('Ctrl Pts',(168.516145661847,-0.752419121938149,
340.870816655879));
#23463=CARTESIAN_POINT('Ctrl Pts',(168.523559219427,-0.907696448716301,
340.846709991054));
#23464=CARTESIAN_POINT('Ctrl Pts',(168.530983331563,-1.06319484119689,340.822569005978));
#23465=CARTESIAN_POINT('Ctrl Pts',(168.5384074437,-1.21755237279293,340.792247856947));
#23466=CARTESIAN_POINT('Ctrl Pts',(168.545831555837,-1.37025146881332,340.755896235576));
#23467=CARTESIAN_POINT('Ctrl Pts',(168.549688680991,-1.44958479696107,340.737010104733));
#23468=CARTESIAN_POINT('Ctrl Pts',(168.553545806146,-1.52847075111401,340.716497030356));
#23469=CARTESIAN_POINT('Ctrl Pts',(168.557402931301,-1.60683879090904,340.694383167871));
#23470=CARTESIAN_POINT('Ctrl Pts',(168.564826908739,-1.75767718374787,340.651819649817));
#23471=CARTESIAN_POINT('Ctrl Pts',(168.572250886177,-1.90705075965012,340.603194451312));
#23472=CARTESIAN_POINT('Ctrl Pts',(168.579674863615,-2.05443511721323,340.54862387549));
#23473=CARTESIAN_POINT('Ctrl Pts',(168.587090079642,-2.20164553905876,340.494117701158));
#23474=CARTESIAN_POINT('Ctrl Pts',(168.59450529567,-2.34687106886702,340.433680244172));
#23475=CARTESIAN_POINT('Ctrl Pts',(168.601920511698,-2.48959997408339,340.367478228325));
#23476=CARTESIAN_POINT('Ctrl Pts',(168.609328592842,-2.63219154626606,340.301339911725));
#23477=CARTESIAN_POINT('Ctrl Pts',(168.616736673986,-2.77229093996604,340.229448234557));
#23478=CARTESIAN_POINT('Ctrl Pts',(168.62414475513,-2.90940411301229,340.152018853778));
#23479=CARTESIAN_POINT('Ctrl Pts',(168.631547322304,-3.04641523022074,340.074647105101));
#23480=CARTESIAN_POINT('Ctrl Pts',(168.638949889478,-3.18044422890968,339.991746042675));
#23481=CARTESIAN_POINT('Ctrl Pts',(168.646352456652,-3.31101960045029,339.90357826163));
#23482=CARTESIAN_POINT('Ctrl Pts',(168.653751126407,-3.44152622462612,339.815456900539));
#23483=CARTESIAN_POINT('Ctrl Pts',(168.661149796161,-3.56858253442073,339.722074551555));
#23484=CARTESIAN_POINT('Ctrl Pts',(168.668548465916,-3.69174416811905,339.623738266777));
#23485=CARTESIAN_POINT('Ctrl Pts',(168.67594591512,-3.81488548397373,339.525418204431));
#23486=CARTESIAN_POINT('Ctrl Pts',(168.683343364324,-3.93413310751987,339.422146060897));
#23487=CARTESIAN_POINT('Ctrl Pts',(168.690740813528,-4.0490739829583,339.314270557467));
#23488=CARTESIAN_POINT('Ctrl Pts',(168.698137941991,-4.16400987476056,339.206399731332));
#23489=CARTESIAN_POINT('Ctrl Pts',(168.705535070455,-4.27463911761045,339.093926197564));
#23490=CARTESIAN_POINT('Ctrl Pts',(168.712932198918,-4.3805841154613,338.977236901401));
#23491=CARTESIAN_POINT('Ctrl Pts',(168.720330466355,-4.48654542619685,338.860529638));
#23492=CARTESIAN_POINT('Ctrl Pts',(168.727728733792,-4.58782080492842,338.739605596047));
#23493=CARTESIAN_POINT('Ctrl Pts',(168.735127001228,-4.68407179482079,338.614886164662));
#23494=CARTESIAN_POINT('Ctrl Pts',(168.742527867754,-4.78035659869837,338.490122918029));
#23495=CARTESIAN_POINT('Ctrl Pts',(168.74992873428,-4.87161327151175,338.361561922517));
#23496=CARTESIAN_POINT('Ctrl Pts',(168.757329600805,-4.95754576233568,338.229654869618));
#23497=CARTESIAN_POINT('Ctrl Pts',(168.76473859419,-5.04357261525004,338.097602970164));
#23498=CARTESIAN_POINT('Ctrl Pts',(168.772147587575,-5.12426340664172,337.962197988463));
#23499=CARTESIAN_POINT('Ctrl Pts',(168.77955658096,-5.199366909167,337.823918254192));
#23500=CARTESIAN_POINT('Ctrl Pts',(168.78697013854,-5.27451667804029,337.685553334835));
#23501=CARTESIAN_POINT('Ctrl Pts',(168.79438369612,-5.34407213498622,337.544310468096));
#23502=CARTESIAN_POINT('Ctrl Pts',(168.8017972537,-5.40782979757288,337.400688951735));
#23503=CARTESIAN_POINT('Ctrl Pts',(168.809221365837,-5.47167823086492,337.256862963851));
#23504=CARTESIAN_POINT('Ctrl Pts',(168.816645477974,-5.52971224715164,337.11065190889));
#23505=CARTESIAN_POINT('Ctrl Pts',(168.824069590111,-5.58177763594187,336.962572033175));
#23506=CARTESIAN_POINT('Ctrl Pts',(168.827926715265,-5.6088277016056,336.885638575946));
#23507=CARTESIAN_POINT('Ctrl Pts',(168.83178384042,-5.63426753600211,336.808200892553));
#23508=CARTESIAN_POINT('Ctrl Pts',(168.835640965575,-5.65808096035101,336.730332456094));
#23509=CARTESIAN_POINT('Ctrl Pts',(168.844722579275,-5.71414974530112,336.546990969619));
#23510=CARTESIAN_POINT('Ctrl Pts',(168.853804192976,-5.76133633025571,336.360814347924));
#23511=CARTESIAN_POINT('Ctrl Pts',(168.862885806677,-5.79939577498008,336.172578017721));
#23512=CARTESIAN_POINT('Ctrl Pts',(168.872121767402,-5.83810206092365,335.981142507441));
#23513=CARTESIAN_POINT('Ctrl Pts',(168.881357728128,-5.86736807475161,335.78757655681));
#23514=CARTESIAN_POINT('Ctrl Pts',(168.890593688854,-5.8869869065239,335.592718925728));
#23515=CARTESIAN_POINT('Ctrl Pts',(168.89982964958,-5.90660573829619,335.397861294646));
#23516=CARTESIAN_POINT('Ctrl Pts',(168.909065610306,-5.91657720739726,335.201711926091));
#23517=CARTESIAN_POINT('Ctrl Pts',(168.918301571032,-5.91674777277373,335.005133797532));
#23518=CARTESIAN_POINT('',(170.668301648409,-5.91237984572483,334.997288801065));
#23519=CARTESIAN_POINT('Ctrl Pts',(168.918301620294,-5.91303584273221,335.005129528958));
#23520=CARTESIAN_POINT('Ctrl Pts',(168.983494080146,-5.90159674938227,333.618433153161));
#23521=CARTESIAN_POINT('Ctrl Pts',(169.141432551421,-4.72234553782323,330.241434468658));
#23522=CARTESIAN_POINT('Ctrl Pts',(169.392117034123,0.909681900777421,328.062774202851));
#23523=CARTESIAN_POINT('Ctrl Pts',(169.670355068396,6.32594224609055,332.010839980807));
#23524=CARTESIAN_POINT('Ctrl Pts',(169.948593102671,5.93697876292119,338.702013788446));
#23525=CARTESIAN_POINT('Ctrl Pts',(170.226831136945,0.0997374986817368,
341.995904184061));
#23526=CARTESIAN_POINT('Ctrl Pts',(170.466733976153,-5.01217502092496,339.300472229507));
#23527=CARTESIAN_POINT('Ctrl Pts',(170.613890803935,-5.90338482414133,336.157054398344));
#23528=CARTESIAN_POINT('Ctrl Pts',(170.668301620294,-5.90816417193379,334.997291333922));
#23529=CARTESIAN_POINT('',(172.418301620294,-5.91993927450693,334.996002217447));
#23530=CARTESIAN_POINT('Ctrl Pts',(170.668301677549,-5.91674937762772,334.997286175768));
#23531=CARTESIAN_POINT('Ctrl Pts',(170.676397060957,-5.91667011842481,334.824483223407));
#23532=CARTESIAN_POINT('Ctrl Pts',(170.684492444364,-5.90901649277877,334.651929759933));
#23533=CARTESIAN_POINT('Ctrl Pts',(170.692587827772,-5.89387862062504,334.48026413647));
#23534=CARTESIAN_POINT('Ctrl Pts',(170.700721293948,-5.87866953602089,334.307790953691));
#23535=CARTESIAN_POINT('Ctrl Pts',(170.708854760125,-5.85590570417694,334.136214224814));
#23536=CARTESIAN_POINT('Ctrl Pts',(170.716988226301,-5.82572901074834,333.966166330677));
#23537=CARTESIAN_POINT('Ctrl Pts',(170.725140880512,-5.7954811260924,333.795717268722));
#23538=CARTESIAN_POINT('Ctrl Pts',(170.733293534724,-5.75778547547219,333.626804490581));
#23539=CARTESIAN_POINT('Ctrl Pts',(170.741446188935,-5.71283407193777,333.460046289979));
#23540=CARTESIAN_POINT('Ctrl Pts',(170.749627290116,-5.66772581994414,333.292706221743));
#23541=CARTESIAN_POINT('Ctrl Pts',(170.757808391298,-5.61531120803269,333.127536016234));
#23542=CARTESIAN_POINT('Ctrl Pts',(170.76598949248,-5.55583196071568,332.965138386329));
#23543=CARTESIAN_POINT('Ctrl Pts',(170.771762063484,-5.51386350551883,332.85055089637));
#23544=CARTESIAN_POINT('Ctrl Pts',(170.777534634488,-5.46837878791062,332.737343328152));
#23545=CARTESIAN_POINT('Ctrl Pts',(170.783307205492,-5.41947643066687,332.625719944921));
#23546=CARTESIAN_POINT('Ctrl Pts',(170.79073118293,-5.35658417752928,332.482163550711));
#23547=CARTESIAN_POINT('Ctrl Pts',(170.798155160368,-5.28788911591296,332.340891247634));
#23548=CARTESIAN_POINT('Ctrl Pts',(170.805579137806,-5.21357852398914,332.202406474003));
#23549=CARTESIAN_POINT('Ctrl Pts',(170.812994353834,-5.13935562974441,332.064085133241));
#23550=CARTESIAN_POINT('Ctrl Pts',(170.820409569861,-5.05953057142885,331.928545099377));
#23551=CARTESIAN_POINT('Ctrl Pts',(170.827824785889,-4.97433882798822,331.796270331806));
#23552=CARTESIAN_POINT('Ctrl Pts',(170.835232867033,-4.88922905561418,331.66412283835));
#23553=CARTESIAN_POINT('Ctrl Pts',(170.842640948177,-4.79876307900438,331.535234668074));
#23554=CARTESIAN_POINT('Ctrl Pts',(170.850049029321,-4.70322241428641,331.410065532039));
#23555=CARTESIAN_POINT('Ctrl Pts',(170.857451596495,-4.60775286223001,331.284989561678));
#23556=CARTESIAN_POINT('Ctrl Pts',(170.864854163669,-4.50721636845959,331.163627409172));
#23557=CARTESIAN_POINT('Ctrl Pts',(170.872256730843,-4.40193784454133,331.046410014266));
#23558=CARTESIAN_POINT('Ctrl Pts',(170.879655400598,-4.29671474930606,330.929254333807));
#23559=CARTESIAN_POINT('Ctrl Pts',(170.887054070353,-4.18675484491862,330.816239341935));
#23560=CARTESIAN_POINT('Ctrl Pts',(170.894452740108,-4.07242334661865,330.707762978537));
#23561=CARTESIAN_POINT('Ctrl Pts',(170.901850189311,-3.95811070946542,330.599304510371));
#23562=CARTESIAN_POINT('Ctrl Pts',(170.909247638515,-3.83942818018199,330.495383441311));
#23563=CARTESIAN_POINT('Ctrl Pts',(170.916645087719,-3.71677794471765,330.396360975037));
#23564=CARTESIAN_POINT('Ctrl Pts',(170.924042216183,-3.59413302715377,330.297342802204));
#23565=CARTESIAN_POINT('Ctrl Pts',(170.931439344646,-3.46752103585102,330.203223044289));
#23566=CARTESIAN_POINT('Ctrl Pts',(170.93883647311,-3.33737714397006,330.114322527898));
#23567=CARTESIAN_POINT('Ctrl Pts',(170.946234740546,-3.20721321317848,330.025408323046));
#23568=CARTESIAN_POINT('Ctrl Pts',(170.953633007983,-3.07351660717547,329.941715170383));
#23569=CARTESIAN_POINT('Ctrl Pts',(170.96103127542,-2.93675123640743,329.863520394476));
#23570=CARTESIAN_POINT('Ctrl Pts',(170.968432141945,-2.79993781852641,329.785298147923));
#23571=CARTESIAN_POINT('Ctrl Pts',(170.975833008471,-2.66005381319633,329.712578309139));
#23572=CARTESIAN_POINT('Ctrl Pts',(170.983233874997,-2.51758731694154,329.645592034214));
#23573=CARTESIAN_POINT('Ctrl Pts',(170.990642868382,-2.37496437885351,329.578532201954));
#23574=CARTESIAN_POINT('Ctrl Pts',(170.998051861766,-2.22975362449477,329.5172186659));
#23575=CARTESIAN_POINT('Ctrl Pts',(171.005460855151,-2.08246337475019,329.461834522577));
#23576=CARTESIAN_POINT('Ctrl Pts',(171.012874412731,-1.93508238913122,329.40641626071));
#23577=CARTESIAN_POINT('Ctrl Pts',(171.020287970312,-1.78561970895525,329.356934787105));
#23578=CARTESIAN_POINT('Ctrl Pts',(171.027701527892,-1.63459786164334,329.313523024472));
#23579=CARTESIAN_POINT('Ctrl Pts',(171.035125640029,-1.48336100708356,329.270049457248));
#23580=CARTESIAN_POINT('Ctrl Pts',(171.042549752165,-1.33056091362334,329.232662947951));
#23581=CARTESIAN_POINT('Ctrl Pts',(171.049973864302,-1.17673012396027,329.20144528543));
#23582=CARTESIAN_POINT('Ctrl Pts',(171.053830989457,-1.09680883539672,329.185226452906));
#23583=CARTESIAN_POINT('Ctrl Pts',(171.057688114612,-1.01660943249272,329.17067187432));
#23584=CARTESIAN_POINT('Ctrl Pts',(171.061545239767,-0.936206914765374,
329.157787476029));
#23585=CARTESIAN_POINT('Ctrl Pts',(171.068969217205,-0.781452673303419,
329.132988311269));
#23586=CARTESIAN_POINT('Ctrl Pts',(171.076393194643,-0.625478940170516,
329.114304904729));
#23587=CARTESIAN_POINT('Ctrl Pts',(171.083817172081,-0.468810414350018,
329.101852209558));
#23588=CARTESIAN_POINT('Ctrl Pts',(171.091232388108,-0.312326780961899,
329.089414210441));
#23589=CARTESIAN_POINT('Ctrl Pts',(171.098647604136,-0.155150355449397,
329.083192315362));
#23590=CARTESIAN_POINT('Ctrl Pts',(171.106062820163,0.00218445923684952,
329.08325040325));
#23591=CARTESIAN_POINT('Ctrl Pts',(171.113470901307,0.15936788715658,329.083308435247));
#23592=CARTESIAN_POINT('Ctrl Pts',(171.120878982452,0.316709030130614,329.089634420447));
#23593=CARTESIAN_POINT('Ctrl Pts',(171.128287063596,0.473668962790444,329.102240401967));
#23594=CARTESIAN_POINT('Ctrl Pts',(171.13568963077,0.630512067305668,329.114837000625));
#23595=CARTESIAN_POINT('Ctrl Pts',(171.143092197944,0.786974156057978,329.133704258609));
#23596=CARTESIAN_POINT('Ctrl Pts',(171.150494765118,0.942517014330444,329.158802157074));
#23597=CARTESIAN_POINT('Ctrl Pts',(171.157893434872,1.09797797996798,329.183886841606));
#23598=CARTESIAN_POINT('Ctrl Pts',(171.165292104627,1.25252031146456,329.215195574197));
#23599=CARTESIAN_POINT('Ctrl Pts',(171.172690774382,1.40561173375845,329.252636585666));
#23600=CARTESIAN_POINT('Ctrl Pts',(171.180088223586,1.55867790072137,329.290071420531));
#23601=CARTESIAN_POINT('Ctrl Pts',(171.18748567279,1.71029327134949,329.333636437929));
#23602=CARTESIAN_POINT('Ctrl Pts',(171.194883121994,1.85993645587018,329.383188899151));
#23603=CARTESIAN_POINT('Ctrl Pts',(171.202280250457,2.00957315212322,329.432739211864));
#23604=CARTESIAN_POINT('Ctrl Pts',(171.20967737892,2.15723747799994,329.4882763349));
#23605=CARTESIAN_POINT('Ctrl Pts',(171.217074507384,2.3024241463946,329.549607939552));
#23606=CARTESIAN_POINT('Ctrl Pts',(171.22447277482,2.44763316991191,329.610948987739));
#23607=CARTESIAN_POINT('Ctrl Pts',(171.231871042257,2.59036343251988,329.678086148801));
#23608=CARTESIAN_POINT('Ctrl Pts',(171.239269309694,2.73013067750983,329.750779386783));
#23609=CARTESIAN_POINT('Ctrl Pts',(171.246670176219,2.86994702420269,329.823498162664));
#23610=CARTESIAN_POINT('Ctrl Pts',(171.254071042745,3.00679794987236,329.901776729612));
#23611=CARTESIAN_POINT('Ctrl Pts',(171.261471909271,3.14022493339615,329.985329728668));
#23612=CARTESIAN_POINT('Ctrl Pts',(171.268880902655,3.27379843250413,330.068974476906));
#23613=CARTESIAN_POINT('Ctrl Pts',(171.27628989604,3.40394016441382,330.157905025653));
#23614=CARTESIAN_POINT('Ctrl Pts',(171.283698889425,3.53022107775309,330.25179300107));
#23615=CARTESIAN_POINT('Ctrl Pts',(171.291112447005,3.65657978449077,330.345738814718));
#23616=CARTESIAN_POINT('Ctrl Pts',(171.298526004585,3.77907264369696,330.44464790651));
#23617=CARTESIAN_POINT('Ctrl Pts',(171.305939562166,3.89730510825632,330.548152804098));
#23618=CARTESIAN_POINT('Ctrl Pts',(171.313363674302,4.01570589837432,330.651805059857));
#23619=CARTESIAN_POINT('Ctrl Pts',(171.320787786439,4.12983390988703,330.760065932877));
#23620=CARTESIAN_POINT('Ctrl Pts',(171.328211898576,4.23933217539608,330.872531857282));
#23621=CARTESIAN_POINT('Ctrl Pts',(171.33206902373,4.29622093280032,330.930962432963));
#23622=CARTESIAN_POINT('Ctrl Pts',(171.335926148885,4.35186068719005,330.990527504226));
#23623=CARTESIAN_POINT('Ctrl Pts',(171.339783274039,4.40620586842443,331.05116720947));
#23624=CARTESIAN_POINT('Ctrl Pts',(171.347207251477,4.51080641498988,331.167883101625));
#23625=CARTESIAN_POINT('Ctrl Pts',(171.354631228915,4.61092402691169,331.288934078038));
#23626=CARTESIAN_POINT('Ctrl Pts',(171.362055206353,4.70617809290688,331.413941115885));
#23627=CARTESIAN_POINT('Ctrl Pts',(171.369470422381,4.80131974477244,331.538800626618));
#23628=CARTESIAN_POINT('Ctrl Pts',(171.376885638409,4.89160905170896,331.667606611604));
#23629=CARTESIAN_POINT('Ctrl Pts',(171.384300854436,4.97670310046095,331.799944248554));
#23630=CARTESIAN_POINT('Ctrl Pts',(171.39170893558,5.06171527214768,331.932154550896));
#23631=CARTESIAN_POINT('Ctrl Pts',(171.399117016725,5.14154193692978,332.067889428326));
#23632=CARTESIAN_POINT('Ctrl Pts',(171.406525097869,5.21588132405397,332.206702204224));
#23633=CARTESIAN_POINT('Ctrl Pts',(171.413927665043,5.29016537901464,332.345411659239));
#23634=CARTESIAN_POINT('Ctrl Pts',(171.421330232217,5.35897011327729,332.487194123541));
#23635=CARTESIAN_POINT('Ctrl Pts',(171.428732799391,5.42203792067594,332.6315753444));
#23636=CARTESIAN_POINT('Ctrl Pts',(171.436131469145,5.4850725231496,332.775880549178));
#23637=CARTESIAN_POINT('Ctrl Pts',(171.4435301389,5.54237606518131,332.922781444449));
#23638=CARTESIAN_POINT('Ctrl Pts',(171.450928808655,5.59373767285501,333.071780767189));
#23639=CARTESIAN_POINT('Ctrl Pts',(171.458326257859,5.64509080745834,333.220755509667));
#23640=CARTESIAN_POINT('Ctrl Pts',(171.465723707063,5.69050383164459,333.371827640075));
#23641=CARTESIAN_POINT('Ctrl Pts',(171.473121156267,5.72981462351643,333.524481466522));
#23642=CARTESIAN_POINT('Ctrl Pts',(171.48051828473,5.76912371094086,333.677128674165));
#23643=CARTESIAN_POINT('Ctrl Pts',(171.487915413194,5.80233099905596,333.83135708007));
#23644=CARTESIAN_POINT('Ctrl Pts',(171.495312541657,5.82932478132986,333.986637697428));
#23645=CARTESIAN_POINT('Ctrl Pts',(171.502710809094,5.85632271997239,334.141942224125));
#23646=CARTESIAN_POINT('Ctrl Pts',(171.510109076531,5.87710518388487,334.298298917149));
#23647=CARTESIAN_POINT('Ctrl Pts',(171.517507343967,5.89161196533026,334.455170657474));
#23648=CARTESIAN_POINT('Ctrl Pts',(171.524908210493,5.90612384316053,334.612097508491));
#23649=CARTESIAN_POINT('Ctrl Pts',(171.532309077019,5.91435561459879,334.769539395672));
#23650=CARTESIAN_POINT('Ctrl Pts',(171.539709943545,5.91629911199055,334.926956314716));
#23651=CARTESIAN_POINT('Ctrl Pts',(171.547118936929,5.91824474352825,335.084546092588));
#23652=CARTESIAN_POINT('Ctrl Pts',(171.554527930314,5.91388830650375,335.242110474164));
#23653=CARTESIAN_POINT('Ctrl Pts',(171.561936923699,5.90327375316903,335.399110959065));
#23654=CARTESIAN_POINT('Ctrl Pts',(171.569350481279,5.89265266090333,335.55620816168));
#23655=CARTESIAN_POINT('Ctrl Pts',(171.576764038859,5.87576581023745,335.712740405228));
#23656=CARTESIAN_POINT('Ctrl Pts',(171.58417759644,5.85270870442605,335.86817704625));
#23657=CARTESIAN_POINT('Ctrl Pts',(171.591601708576,5.82961877260337,336.023834979787));
#23658=CARTESIAN_POINT('Ctrl Pts',(171.599025820713,5.80034111052963,336.178393829881));
#23659=CARTESIAN_POINT('Ctrl Pts',(171.60644993285,5.76502190981836,336.33133502238));
#23660=CARTESIAN_POINT('Ctrl Pts',(171.610307058004,5.74667216307458,336.410794129396));
#23661=CARTESIAN_POINT('Ctrl Pts',(171.614164183159,5.72669248759253,336.489816863788));
#23662=CARTESIAN_POINT('Ctrl Pts',(171.618021308314,5.70510856165326,336.568332510104));
#23663=CARTESIAN_POINT('Ctrl Pts',(171.625445285752,5.66356503564055,336.719455007668));
#23664=CARTESIAN_POINT('Ctrl Pts',(171.63286926319,5.61595007162408,336.869153672689));
#23665=CARTESIAN_POINT('Ctrl Pts',(171.640293240628,5.56237642737782,337.016903330021));
#23666=CARTESIAN_POINT('Ctrl Pts',(171.647708456655,5.50886600809237,337.164478620528));
#23667=CARTESIAN_POINT('Ctrl Pts',(171.655123672683,5.44941103214534,337.310109134331));
#23668=CARTESIAN_POINT('Ctrl Pts',(171.662538888711,5.38417476240957,337.453282024214));
#23669=CARTESIAN_POINT('Ctrl Pts',(171.669946969855,5.31900126268406,337.596317153863));
#23670=CARTESIAN_POINT('Ctrl Pts',(171.677355050999,5.24805769724341,337.736899029949));
#23671=CARTESIAN_POINT('Ctrl Pts',(171.684763132143,5.17155638051572,337.874532164657));
#23672=CARTESIAN_POINT('Ctrl Pts',(171.692165699317,5.09511200511524,338.012062856509));
#23673=CARTESIAN_POINT('Ctrl Pts',(171.699568266491,5.01311829581158,338.146648852345));
#23674=CARTESIAN_POINT('Ctrl Pts',(171.706970833665,4.92583465636595,338.277816880279));
#23675=CARTESIAN_POINT('Ctrl Pts',(171.71436950342,4.838596971375,338.40891584882));
#23676=CARTESIAN_POINT('Ctrl Pts',(171.721768173175,4.74607510921836,338.536600123435));
#23677=CARTESIAN_POINT('Ctrl Pts',(171.729166842929,4.64857311300592,338.660423278193));
#23678=CARTESIAN_POINT('Ctrl Pts',(171.736564292133,4.55108720159523,338.784226005976));
#23679=CARTESIAN_POINT('Ctrl Pts',(171.743961741337,4.44862301733904,338.904168585139));
#23680=CARTESIAN_POINT('Ctrl Pts',(171.751359190541,4.3415264830876,339.019835613448));
#23681=CARTESIAN_POINT('Ctrl Pts',(171.758756319005,4.23443459235523,339.135497626637));
#23682=CARTESIAN_POINT('Ctrl Pts',(171.766153447468,4.12271100454429,339.246884183718));
#23683=CARTESIAN_POINT('Ctrl Pts',(171.773550575932,4.00674010513229,339.353615083172));
#23684=CARTESIAN_POINT('Ctrl Pts',(171.780948843368,3.89075134909677,339.46036241652));
#23685=CARTESIAN_POINT('Ctrl Pts',(171.788347110805,3.77051425393001,339.562452412139));
#23686=CARTESIAN_POINT('Ctrl Pts',(171.795745378241,3.64644791261821,339.659543774133));
#23687=CARTESIAN_POINT('Ctrl Pts',(171.803146244767,3.52233798549585,339.756669245344));
#23688=CARTESIAN_POINT('Ctrl Pts',(171.810547111293,3.39439642755439,339.848792356731));
#23689=CARTESIAN_POINT('Ctrl Pts',(171.817947977819,3.26307291994351,339.935614012626));
#23690=CARTESIAN_POINT('Ctrl Pts',(171.825356971203,3.1316052065663,340.022531007));
#23691=CARTESIAN_POINT('Ctrl Pts',(171.832765964588,2.99674843856413,340.104134714079));
#23692=CARTESIAN_POINT('Ctrl Pts',(171.840174957973,2.85897923748019,340.180170680794));
#23693=CARTESIAN_POINT('Ctrl Pts',(171.847588515553,2.72112516581621,340.256253488287));
#23694=CARTESIAN_POINT('Ctrl Pts',(171.855002073133,2.58035541888477,340.3267615541));
#23695=CARTESIAN_POINT('Ctrl Pts',(171.862415630714,2.43716790838336,340.39148802733));
#23696=CARTESIAN_POINT('Ctrl Pts',(171.86983974285,2.29377654424685,340.456306650546));
#23697=CARTESIAN_POINT('Ctrl Pts',(171.877263854987,2.14796088693417,340.515327102267));
#23698=CARTESIAN_POINT('Ctrl Pts',(171.884687967124,2.00023612918477,340.568391687912));
#23699=CARTESIAN_POINT('Ctrl Pts',(171.888545092278,1.92348717003776,340.595960876569));
#23700=CARTESIAN_POINT('Ctrl Pts',(171.892402217433,1.8462231179741,340.621923277112));
#23701=CARTESIAN_POINT('Ctrl Pts',(171.896259342588,1.76851733511725,340.646262214766));
#23702=CARTESIAN_POINT('Ctrl Pts',(171.903683320026,1.61895361716687,340.693108432288));
#23703=CARTESIAN_POINT('Ctrl Pts',(171.911107297464,1.46730162689439,340.734078530576));
#23704=CARTESIAN_POINT('Ctrl Pts',(171.918531274902,1.31406401498585,340.768983127642));
#23705=CARTESIAN_POINT('Ctrl Pts',(171.925946490929,1.16100724651521,340.803846532032));
#23706=CARTESIAN_POINT('Ctrl Pts',(171.933361706957,1.00636894155728,340.832658601637));
#23707=CARTESIAN_POINT('Ctrl Pts',(171.940776922984,0.850668715184559,340.855279096636));
#23708=CARTESIAN_POINT('Ctrl Pts',(171.948185004129,0.695118302785645,340.877877826309));
#23709=CARTESIAN_POINT('Ctrl Pts',(171.955593085273,0.538508370001836,340.894296788351));
#23710=CARTESIAN_POINT('Ctrl Pts',(171.963001166417,0.381370478625698,340.904446385609));
#23711=CARTESIAN_POINT('Ctrl Pts',(171.970403733591,0.22434954785202,340.914588428336));
#23712=CARTESIAN_POINT('Ctrl Pts',(171.977806300765,0.0668018117849019,
340.918470373814));
#23713=CARTESIAN_POINT('Ctrl Pts',(171.985208867939,-0.0907343668901057,
340.916054245624));
#23714=CARTESIAN_POINT('Ctrl Pts',(171.992607537694,-0.2481876034558,340.913639389515));
#23715=CARTESIAN_POINT('Ctrl Pts',(172.000006207448,-0.405628922520294,
340.904933069276));
#23716=CARTESIAN_POINT('Ctrl Pts',(172.007404877203,-0.562518379822016,
340.889949374559));
#23717=CARTESIAN_POINT('Ctrl Pts',(172.014802326407,-0.719381955234808,
340.874968151685));
#23718=CARTESIAN_POINT('Ctrl Pts',(172.022199775611,-0.875693478410385,
340.853711645055));
#23719=CARTESIAN_POINT('Ctrl Pts',(172.029597224815,-1.03091643004478,340.82624595059));
#23720=CARTESIAN_POINT('Ctrl Pts',(172.036994353278,-1.18613265148262,340.798781446989));
#23721=CARTESIAN_POINT('Ctrl Pts',(172.044391481742,-1.340260027723,340.765108355876));
#23722=CARTESIAN_POINT('Ctrl Pts',(172.051788610205,-1.49277082615823,340.725344166342));
#23723=CARTESIAN_POINT('Ctrl Pts',(172.059186877642,-1.64530510744938,340.685573854116));
#23724=CARTESIAN_POINT('Ctrl Pts',(172.066585145079,-1.79622195415762,340.639710670196));
#23725=CARTESIAN_POINT('Ctrl Pts',(172.073983412515,-1.9450075680211,340.587922344024));
#23726=CARTESIAN_POINT('Ctrl Pts',(172.081384279041,-2.0938454518356,340.536115824068));
#23727=CARTESIAN_POINT('Ctrl Pts',(172.088785145567,-2.24055025984838,340.478380140076));
#23728=CARTESIAN_POINT('Ctrl Pts',(172.096186012093,-2.38462712785935,340.414931580692));
#23729=CARTESIAN_POINT('Ctrl Pts',(172.103595005477,-2.52886220604546,340.351413348724));
#23730=CARTESIAN_POINT('Ctrl Pts',(172.111003998862,-2.67046323951235,340.282169863788));
#23731=CARTESIAN_POINT('Ctrl Pts',(172.118412992247,-2.80895832598085,340.207464227952));
#23732=CARTESIAN_POINT('Ctrl Pts',(172.125826549827,-2.94753873019977,340.132712570868));
#23733=CARTESIAN_POINT('Ctrl Pts',(172.133240107407,-3.08300905439576,340.052492247645));
#23734=CARTESIAN_POINT('Ctrl Pts',(172.140653664988,-3.21492590464417,339.967110023962));
#23735=CARTESIAN_POINT('Ctrl Pts',(172.148077777124,-3.34703056267942,339.881606243053));
#23736=CARTESIAN_POINT('Ctrl Pts',(172.155501889261,-3.47557133875071,339.790926098998));
#23737=CARTESIAN_POINT('Ctrl Pts',(172.162926001398,-3.60013682376539,339.695417490774));
#23738=CARTESIAN_POINT('Ctrl Pts',(172.166783126552,-3.66485360831885,339.645796923563));
#23739=CARTESIAN_POINT('Ctrl Pts',(172.170640251707,-3.72849795680047,339.594873678482));
#23740=CARTESIAN_POINT('Ctrl Pts',(172.174497376862,-3.79101614658229,339.54270042363));
#23741=CARTESIAN_POINT('Ctrl Pts',(172.181818212763,-3.9096758710846,339.443675418768));
#23742=CARTESIAN_POINT('Ctrl Pts',(172.189139048664,-4.02465609841748,339.339828283579));
#23743=CARTESIAN_POINT('Ctrl Pts',(172.196459884565,-4.1355316721976,339.231466453932));
#23744=CARTESIAN_POINT('Ctrl Pts',(172.203772028285,-4.24627560109991,339.123233284541));
#23745=CARTESIAN_POINT('Ctrl Pts',(172.211084172005,-4.35292430052376,339.010496351369));
#23746=CARTESIAN_POINT('Ctrl Pts',(172.218396315725,-4.45508423787825,338.893604370748));
#23747=CARTESIAN_POINT('Ctrl Pts',(172.225701478377,-4.55714664083613,338.776823989538));
#23748=CARTESIAN_POINT('Ctrl Pts',(172.233006641028,-4.65472855823844,338.655896742196));
#23749=CARTESIAN_POINT('Ctrl Pts',(172.24031180368,-4.74747221290994,338.531209162617));
#23750=CARTESIAN_POINT('Ctrl Pts',(172.247728046039,-4.84162609463798,338.404625628009));
#23751=CARTESIAN_POINT('Ctrl Pts',(172.255144288398,-4.93079307559503,338.274166738327));
#23752=CARTESIAN_POINT('Ctrl Pts',(172.262560530756,-5.01463975739856,338.140273661008));
#23753=CARTESIAN_POINT('Ctrl Pts',(172.269857201924,-5.09713458914619,338.008539325813));
#23754=CARTESIAN_POINT('Ctrl Pts',(172.277153873091,-5.17447917821394,337.873481047779));
#23755=CARTESIAN_POINT('Ctrl Pts',(172.284450544259,-5.24639872171483,337.735549490557));
#23756=CARTESIAN_POINT('Ctrl Pts',(172.291745787673,-5.31830419258919,337.597644922652));
#23757=CARTESIAN_POINT('Ctrl Pts',(172.299041031088,-5.38478655221305,337.456868534898));
#23758=CARTESIAN_POINT('Ctrl Pts',(172.306336274503,-5.44561666873498,337.313696103575));
#23759=CARTESIAN_POINT('Ctrl Pts',(172.31363162386,-5.50644766864442,337.170521593071));
#23760=CARTESIAN_POINT('Ctrl Pts',(172.320926973218,-5.56162611251567,337.024951323964));
#23761=CARTESIAN_POINT('Ctrl Pts',(172.328222322576,-5.61097090855777,336.877481298394));
#23762=CARTESIAN_POINT('Ctrl Pts',(172.335728930719,-5.66174463160155,336.725740834634));
#23763=CARTESIAN_POINT('Ctrl Pts',(172.343235538862,-5.70634157861289,336.571989327393));
#23764=CARTESIAN_POINT('Ctrl Pts',(172.350742147005,-5.74461968890823,336.416783396398));
#23765=CARTESIAN_POINT('Ctrl Pts',(172.358045506196,-5.78186138093522,336.265779821814));
#23766=CARTESIAN_POINT('Ctrl Pts',(172.365348865387,-5.81312196157397,336.113399956991));
#23767=CARTESIAN_POINT('Ctrl Pts',(172.372652224578,-5.83832275100674,335.960165619868));
#23768=CARTESIAN_POINT('Ctrl Pts',(172.380260457197,-5.86457552910289,335.800534626564));
#23769=CARTESIAN_POINT('Ctrl Pts',(172.387868689817,-5.88425161840677,335.6399767522));
#23770=CARTESIAN_POINT('Ctrl Pts',(172.395476922436,-5.89732206354305,335.479085630497));
#23771=CARTESIAN_POINT('Ctrl Pts',(172.403085155055,-5.91039250867933,335.318194508793));
#23772=CARTESIAN_POINT('Ctrl Pts',(172.410693387675,-5.91685735265219,335.156970607304));
#23773=CARTESIAN_POINT('Ctrl Pts',(172.418301620294,-5.91674865086034,334.9960043721));
#23774=CARTESIAN_POINT('',(174.168301620294,-5.92071488197934,335.004845951965));
#23775=CARTESIAN_POINT('Ctrl Pts',(172.418301620294,-5.92297626124348,334.996000166545));
#23776=CARTESIAN_POINT('Ctrl Pts',(172.429779550575,-5.92486170322552,334.752906339495));
#23777=CARTESIAN_POINT('Ctrl Pts',(172.534003492275,-5.80077126720912,332.547462997274));
#23778=CARTESIAN_POINT('Ctrl Pts',(172.730973445414,-3.03182805015908,328.694396016598));
#23779=CARTESIAN_POINT('Ctrl Pts',(173.009211479682,3.66182078960602,329.038146980508));
#23780=CARTESIAN_POINT('Ctrl Pts',(173.287449513959,6.99507073913546,334.853002463598));
#23781=CARTESIAN_POINT('Ctrl Pts',(173.565687548231,3.9090475184357,340.802755416165));
#23782=CARTESIAN_POINT('Ctrl Pts',(173.843925582506,-2.7642509124862,341.427405371847));
#23783=CARTESIAN_POINT('Ctrl Pts',(174.04479693986,-5.75062076917938,337.620117542955));
#23784=CARTESIAN_POINT('Ctrl Pts',(174.152922285789,-5.92360130403154,335.330892503762));
#23785=CARTESIAN_POINT('Ctrl Pts',(174.168301620294,-5.92071488197934,335.004845951965));
#23786=CARTESIAN_POINT('',(175.918301620294,-5.90728851166745,335.001439949397));
#23787=CARTESIAN_POINT('Ctrl Pts',(174.168301620294,-5.92071488197934,335.004845951965));
#23788=CARTESIAN_POINT('Ctrl Pts',(174.245668297214,-5.90619456042088,333.364648957377));
#23789=CARTESIAN_POINT('Ctrl Pts',(174.415780985559,-4.34459534383266,329.7339498889));
#23790=CARTESIAN_POINT('Ctrl Pts',(174.678639685327,1.80894992907605,328.24127799985));
#23791=CARTESIAN_POINT('Ctrl Pts',(174.956877719602,6.66248012508402,332.863652297945));
#23792=CARTESIAN_POINT('Ctrl Pts',(175.235115753876,5.40195064834963,339.446521349778));
#23793=CARTESIAN_POINT('Ctrl Pts',(175.513353788148,-0.815869205717351,
341.948883389464));
#23794=CARTESIAN_POINT('Ctrl Pts',(175.741082410288,-5.29215368564465,338.777712355323));
#23795=CARTESIAN_POINT('Ctrl Pts',(175.876065021004,-5.90924419443841,335.902043646341));
#23796=CARTESIAN_POINT('Ctrl Pts',(175.918301620294,-5.90728851166745,335.001439949397));
#23797=CARTESIAN_POINT('',(177.66830162302,-5.91560657051319,334.994568519548));
#23798=CARTESIAN_POINT('Ctrl Pts',(175.918301620294,-5.90728851166745,335.001439949397));
#23799=CARTESIAN_POINT('Ctrl Pts',(175.968811032428,-5.90494977254684,333.924436495925));
#23800=CARTESIAN_POINT('Ctrl Pts',(176.112066455989,-5.10719719425614,330.866599509878));
#23801=CARTESIAN_POINT('Ctrl Pts',(176.348067890969,-0.194250865120091,
328.006081961981));
#23802=CARTESIAN_POINT('Ctrl Pts',(176.626305925245,5.77621459762169,331.051839942032));
#23803=CARTESIAN_POINT('Ctrl Pts',(176.904543959518,6.44593318097529,337.720766132576));
#23804=CARTESIAN_POINT('Ctrl Pts',(177.182781993793,1.20031402584974,341.892885401616));
#23805=CARTESIAN_POINT('Ctrl Pts',(177.437367880718,-4.60726590443529,339.922557586672));
#23806=CARTESIAN_POINT('Ctrl Pts',(177.599207756218,-5.90217096337117,336.462749761299));
#23807=CARTESIAN_POINT('Ctrl Pts',(177.668301620294,-5.91541773274628,334.994568750865));
#23808=CARTESIAN_POINT('',(179.418302336057,-5.92193779621029,335.001244208886));
#23809=CARTESIAN_POINT('Ctrl Pts',(177.668301639489,-5.91674750571091,334.994567121961));
#23810=CARTESIAN_POINT('Ctrl Pts',(177.677735650211,-5.91656339584637,334.794059844961));
#23811=CARTESIAN_POINT('Ctrl Pts',(177.687169660932,-5.90618360898286,334.594007430929));
#23812=CARTESIAN_POINT('Ctrl Pts',(177.696603671654,-5.88576758330674,334.395293031464));
#23813=CARTESIAN_POINT('Ctrl Pts',(177.706233207941,-5.86492842317771,334.19246015615));
#23814=CARTESIAN_POINT('Ctrl Pts',(177.715862744228,-5.83363270039088,333.991021115608));
#23815=CARTESIAN_POINT('Ctrl Pts',(177.725492280515,-5.79209813957887,333.79189002819));
#23816=CARTESIAN_POINT('Ctrl Pts',(177.730080874457,-5.77230640418817,333.697001585573));
#23817=CARTESIAN_POINT('Ctrl Pts',(177.734669468399,-5.75019049164024,333.602636854439));
#23818=CARTESIAN_POINT('Ctrl Pts',(177.739258062341,-5.72577772529589,333.508893027645));
#23819=CARTESIAN_POINT('Ctrl Pts',(177.746682039777,-5.68627982489756,333.357223025097));
#23820=CARTESIAN_POINT('Ctrl Pts',(177.754106017213,-5.64069180312919,333.206894693222));
#23821=CARTESIAN_POINT('Ctrl Pts',(177.761529994649,-5.5891193117699,333.058434682711));
#23822=CARTESIAN_POINT('Ctrl Pts',(177.768945210675,-5.53760768371,332.91014987735));
#23823=CARTESIAN_POINT('Ctrl Pts',(177.7763604267,-5.48012576550352,332.763729353581));
#23824=CARTESIAN_POINT('Ctrl Pts',(177.783775642726,-5.41682987598247,332.61968811767));
#23825=CARTESIAN_POINT('Ctrl Pts',(177.791183723868,-5.3535948894477,332.475785477511));
#23826=CARTESIAN_POINT('Ctrl Pts',(177.79859180501,-5.28455721769547,332.334257906957));
#23827=CARTESIAN_POINT('Ctrl Pts',(177.805999886152,-5.20992246118055,332.195603717199));
#23828=CARTESIAN_POINT('Ctrl Pts',(177.813402453324,-5.13534325667828,332.057052730288));
#23829=CARTESIAN_POINT('Ctrl Pts',(177.820805020496,-5.05517543868624,331.921371192908));
#23830=CARTESIAN_POINT('Ctrl Pts',(177.828207587668,-4.969671992856,331.78903583858));
#23831=CARTESIAN_POINT('Ctrl Pts',(177.83560625742,-4.88421356421617,331.656770158238));
#23832=CARTESIAN_POINT('Ctrl Pts',(177.843004927173,-4.79342530442435,331.527847464999));
#23833=CARTESIAN_POINT('Ctrl Pts',(177.850403596926,-4.69760519712498,331.402718252007));
#23834=CARTESIAN_POINT('Ctrl Pts',(177.857801046128,-4.60180089716821,331.277609681449));
#23835=CARTESIAN_POINT('Ctrl Pts',(177.86519849533,-4.50096662386682,331.156293645137));
#23836=CARTESIAN_POINT('Ctrl Pts',(177.872595944531,-4.39544265594761,331.039190181191));
#23837=CARTESIAN_POINT('Ctrl Pts',(177.879993072993,-4.28992326336374,330.922091794646));
#23838=CARTESIAN_POINT('Ctrl Pts',(177.887390201454,-4.17971483029927,330.80920589455));
#23839=CARTESIAN_POINT('Ctrl Pts',(177.894787329916,-4.06519657019832,330.700917841196));
#23840=CARTESIAN_POINT('Ctrl Pts',(177.90218559735,-3.95066067714397,330.592613114184));
#23841=CARTESIAN_POINT('Ctrl Pts',(177.909583864785,-3.83181390691669,330.488907899979));
#23842=CARTESIAN_POINT('Ctrl Pts',(177.916982132219,-3.70907070295967,330.390149125737));
#23843=CARTESIAN_POINT('Ctrl Pts',(177.924382998743,-3.58628437802431,330.291355656498));
#23844=CARTESIAN_POINT('Ctrl Pts',(177.931783865266,-3.45959918455769,330.197512320861));
#23845=CARTESIAN_POINT('Ctrl Pts',(177.93918473179,-3.32946072154656,330.108924262887));
#23846=CARTESIAN_POINT('Ctrl Pts',(177.946593725173,-3.19917935406093,330.020238926755));
#23847=CARTESIAN_POINT('Ctrl Pts',(177.954002718555,-3.06543745286287,329.936820603013));
#23848=CARTESIAN_POINT('Ctrl Pts',(177.961411711938,-2.92870815804487,329.858930161192));
#23849=CARTESIAN_POINT('Ctrl Pts',(177.968825269516,-2.79189463326487,329.780991736172));
#23850=CARTESIAN_POINT('Ctrl Pts',(177.976238827094,-2.65209037837958,329.708588149946));
#23851=CARTESIAN_POINT('Ctrl Pts',(177.983652384672,-2.50979046485076,329.641932961875));
#23852=CARTESIAN_POINT('Ctrl Pts',(177.991076496807,-2.36728796134321,329.57518287794));
#23853=CARTESIAN_POINT('Ctrl Pts',(177.998500608942,-2.22228304618235,329.514197681338));
#23854=CARTESIAN_POINT('Ctrl Pts',(178.005924721076,-2.07528873445123,329.459142013085));
#23855=CARTESIAN_POINT('Ctrl Pts',(178.009781846256,-1.99891927090797,329.430538376659));
#23856=CARTESIAN_POINT('Ctrl Pts',(178.013638971435,-1.92201305195829,329.403534422221));
#23857=CARTESIAN_POINT('Ctrl Pts',(178.017496096615,-1.84464320773582,329.378147814229));
#23858=CARTESIAN_POINT('Ctrl Pts',(178.02492007406,-1.69572608636336,329.32928510006));
#23859=CARTESIAN_POINT('Ctrl Pts',(178.032344051506,-1.54464149035693,329.286269753881));
#23860=CARTESIAN_POINT('Ctrl Pts',(178.039768028952,-1.39188946576013,329.249297931765));
#23861=CARTESIAN_POINT('Ctrl Pts',(178.047183244987,-1.23931771153463,329.212369741961));
#23862=CARTESIAN_POINT('Ctrl Pts',(178.054598461023,-1.085082804899,329.181470966271));
#23863=CARTESIAN_POINT('Ctrl Pts',(178.062013677058,-0.929702418700275,
329.156748852294));
#23864=CARTESIAN_POINT('Ctrl Pts',(178.06942175821,-0.774471538726483,329.132050525811));
#23865=CARTESIAN_POINT('Ctrl Pts',(178.076829839362,-0.61809773952573,329.113517087583));
#23866=CARTESIAN_POINT('Ctrl Pts',(178.084237920514,-0.461111323813465,
329.10124530858));
#23867=CARTESIAN_POINT('Ctrl Pts',(178.091640487696,-0.304241755957706,
329.088982663685));
#23868=CARTESIAN_POINT('Ctrl Pts',(178.099043054877,-0.146760849998787,
329.082972426909));
#23869=CARTESIAN_POINT('Ctrl Pts',(178.106445622059,0.0107935936219287,
329.083259845081));
#23870=CARTESIAN_POINT('Ctrl Pts',(178.113844291822,0.168265085516562,329.083547111928));
#23871=CARTESIAN_POINT('Ctrl Pts',(178.121242961584,0.325809665694562,329.090125429655));
#23872=CARTESIAN_POINT('Ctrl Pts',(178.128641631347,0.482887248812271,329.102988005147));
#23873=CARTESIAN_POINT('Ctrl Pts',(178.136039080558,0.639938919005676,329.115848458714));
#23874=CARTESIAN_POINT('Ctrl Pts',(178.14343652977,0.796523373433738,329.134991082086));
#23875=CARTESIAN_POINT('Ctrl Pts',(178.150833978982,0.952103248735099,329.160357034351));
#23876=CARTESIAN_POINT('Ctrl Pts',(178.158231107453,1.10767637836364,329.185721886793));
#23877=CARTESIAN_POINT('Ctrl Pts',(178.165628235924,1.26224464712315,329.217309471555));
#23878=CARTESIAN_POINT('Ctrl Pts',(178.173025364395,1.41527878316743,329.255009440529));
#23879=CARTESIAN_POINT('Ctrl Pts',(178.18042363184,1.5683364826479,329.292715214356));
#23880=CARTESIAN_POINT('Ctrl Pts',(178.187821899284,1.71985921667248,329.33653515708));
#23881=CARTESIAN_POINT('Ctrl Pts',(178.195220166728,1.86933096766575,329.386308496557));
#23882=CARTESIAN_POINT('Ctrl Pts',(178.202621033262,2.01885522965619,329.436099321932));
#23883=CARTESIAN_POINT('Ctrl Pts',(178.210021899795,2.16632672016538,329.491847590378));
#23884=CARTESIAN_POINT('Ctrl Pts',(178.217422766329,2.31124769786232,329.553343719159));
#23885=CARTESIAN_POINT('Ctrl Pts',(178.224831759721,2.45632781264585,329.614907376568));
#23886=CARTESIAN_POINT('Ctrl Pts',(178.232240753113,2.59885147769186,329.682231353241));
#23887=CARTESIAN_POINT('Ctrl Pts',(178.239649746506,2.73834327899274,329.755058947052));
#23888=CARTESIAN_POINT('Ctrl Pts',(178.247063304093,2.87792101205398,329.827931405173));
#23889=CARTESIAN_POINT('Ctrl Pts',(178.254476861681,3.01446283675097,329.906314050916));
#23890=CARTESIAN_POINT('Ctrl Pts',(178.261890419269,3.14752125488427,329.989906137351));
#23891=CARTESIAN_POINT('Ctrl Pts',(178.269314531413,3.28076910603264,330.073617232423));
#23892=CARTESIAN_POINT('Ctrl Pts',(178.276738643557,3.41052333895812,330.162552370178));
#23893=CARTESIAN_POINT('Ctrl Pts',(178.284162755701,3.53636788161693,330.256369241987));
#23894=CARTESIAN_POINT('Ctrl Pts',(178.288019880764,3.60174918648625,330.305110882809));
#23895=CARTESIAN_POINT('Ctrl Pts',(178.291877005826,3.66607575385617,330.355169572337));
#23896=CARTESIAN_POINT('Ctrl Pts',(178.295734130889,3.7292931544016,330.406493373137));
#23897=CARTESIAN_POINT('Ctrl Pts',(178.303158108318,3.85097045217884,330.505278538917));
#23898=CARTESIAN_POINT('Ctrl Pts',(178.310582085748,3.96890351837916,330.609050726683));
#23899=CARTESIAN_POINT('Ctrl Pts',(178.318006063177,4.08265679756999,330.717495588355));
#23900=CARTESIAN_POINT('Ctrl Pts',(178.325421279196,4.19627583077655,330.825812468775));
#23901=CARTESIAN_POINT('Ctrl Pts',(178.332836495216,4.3057246282449,330.938790791468));
#23902=CARTESIAN_POINT('Ctrl Pts',(178.340251711235,4.41059922384577,331.056074918421));
#23903=CARTESIAN_POINT('Ctrl Pts',(178.34765979237,4.51537290963921,331.173246195177));
#23904=CARTESIAN_POINT('Ctrl Pts',(178.355067873506,4.61558090857261,331.294714751858));
#23905=CARTESIAN_POINT('Ctrl Pts',(178.362475954642,4.71085486664632,331.420087013921));
#23906=CARTESIAN_POINT('Ctrl Pts',(178.369878521807,4.80605791057351,331.545365959121));
#23907=CARTESIAN_POINT('Ctrl Pts',(178.377281088973,4.89633400127358,331.674542528359));
#23908=CARTESIAN_POINT('Ctrl Pts',(178.384683656138,4.98135405504422,331.807188959429));
#23909=CARTESIAN_POINT('Ctrl Pts',(178.392082325885,5.06632934612877,331.939765552733));
#23910=CARTESIAN_POINT('Ctrl Pts',(178.399480995631,5.14605391060109,332.075808056136));
#23911=CARTESIAN_POINT('Ctrl Pts',(178.406879665378,5.22024118976822,332.214858624208));
#23912=CARTESIAN_POINT('Ctrl Pts',(178.414277114573,5.2944162303389,332.353886253256));
#23913=CARTESIAN_POINT('Ctrl Pts',(178.421674563769,5.36305562305941,332.495920633145));
#23914=CARTESIAN_POINT('Ctrl Pts',(178.429072012965,5.4259180503607,332.640478041367));
#23915=CARTESIAN_POINT('Ctrl Pts',(178.43646914142,5.48877775205724,332.785029181834));
#23916=CARTESIAN_POINT('Ctrl Pts',(178.443866269875,5.54586083753778,332.932102790871));
#23917=CARTESIAN_POINT('Ctrl Pts',(178.451263398331,5.59697368151684,333.0811940768));
#23918=CARTESIAN_POINT('Ctrl Pts',(178.458661665759,5.64809439559847,333.230308319067));
#23919=CARTESIAN_POINT('Ctrl Pts',(178.466059933188,5.69324291675456,333.381440503752));
#23920=CARTESIAN_POINT('Ctrl Pts',(178.473458200616,5.73227519499158,333.534069697638));
#23921=CARTESIAN_POINT('Ctrl Pts',(178.480859067134,5.77132118567885,333.686752511766));
#23922=CARTESIAN_POINT('Ctrl Pts',(178.488259933652,5.80424656297964,333.840933020843));
#23923=CARTESIAN_POINT('Ctrl Pts',(178.495660800169,5.83095821309311,333.996079246324));
#23924=CARTESIAN_POINT('Ctrl Pts',(178.503069793546,5.85769919515275,334.151395837196));
#23925=CARTESIAN_POINT('Ctrl Pts',(178.510478786923,5.878212760235,334.307679894225));
#23926=CARTESIAN_POINT('Ctrl Pts',(178.5178877803,5.89245750083646,334.464392715382));
#23927=CARTESIAN_POINT('Ctrl Pts',(178.525301337873,5.90671101668964,334.621202077044));
#23928=CARTESIAN_POINT('Ctrl Pts',(178.532714895445,5.91468799402555,334.778440357292));
#23929=CARTESIAN_POINT('Ctrl Pts',(178.540128453017,5.91639917040129,334.935568493927));
#23930=CARTESIAN_POINT('Ctrl Pts',(178.547552565147,5.91811278294993,335.092920331234));
#23931=CARTESIAN_POINT('Ctrl Pts',(178.554976677276,5.91354278929872,335.250161339698));
#23932=CARTESIAN_POINT('Ctrl Pts',(178.562400789405,5.90275188361823,335.406756392625));
#23933=CARTESIAN_POINT('Ctrl Pts',(178.566257914657,5.89714557352008,335.488113829391));
#23934=CARTESIAN_POINT('Ctrl Pts',(178.57011503991,5.88986094992002,335.569297045502));
#23935=CARTESIAN_POINT('Ctrl Pts',(178.573972165163,5.88091223328538,335.650232163842));
#23936=CARTESIAN_POINT('Ctrl Pts',(178.58139614259,5.86368824755755,335.806011520824));
#23937=CARTESIAN_POINT('Ctrl Pts',(178.588820120018,5.84024435010495,335.96134103735));
#23938=CARTESIAN_POINT('Ctrl Pts',(178.596244097446,5.81060917889468,336.115684333781));
#23939=CARTESIAN_POINT('Ctrl Pts',(178.603659313463,5.78100898164574,336.269845481898));
#23940=CARTESIAN_POINT('Ctrl Pts',(178.61107452948,5.74523212430144,336.423022363707));
#23941=CARTESIAN_POINT('Ctrl Pts',(178.618489745497,5.70335906120161,336.574682819335));
#23942=CARTESIAN_POINT('Ctrl Pts',(178.625897826631,5.66152628815285,336.726197348035));
#23943=CARTESIAN_POINT('Ctrl Pts',(178.633305907764,5.61360908560313,336.876197997999));
#23944=CARTESIAN_POINT('Ctrl Pts',(178.640713988898,5.55973908129434,337.024162026723));
#23945=CARTESIAN_POINT('Ctrl Pts',(178.648116556061,5.50590917341429,337.172015923117));
#23946=CARTESIAN_POINT('Ctrl Pts',(178.655519123224,5.44613541323306,337.317835867448));
#23947=CARTESIAN_POINT('Ctrl Pts',(178.662921690388,5.38059942904098,337.461113639535));
#23948=CARTESIAN_POINT('Ctrl Pts',(178.670320360132,5.31509794925878,337.6043159765));
#23949=CARTESIAN_POINT('Ctrl Pts',(178.677719029876,5.24384044227906,337.744978468271));
#23950=CARTESIAN_POINT('Ctrl Pts',(178.68511769962,5.16705684673975,337.882612375097));
#23951=CARTESIAN_POINT('Ctrl Pts',(178.692515148813,5.09028591811017,338.0202235766));
#23952=CARTESIAN_POINT('Ctrl Pts',(178.699912598006,5.00799089186809,338.154806859141));
#23953=CARTESIAN_POINT('Ctrl Pts',(178.707310047199,4.92044794980542,338.285897523624));
#23954=CARTESIAN_POINT('Ctrl Pts',(178.714707175652,4.83290880345264,338.416982504242));
#23955=CARTESIAN_POINT('Ctrl Pts',(178.722104304105,4.74012240096959,338.544574857535));
#23956=CARTESIAN_POINT('Ctrl Pts',(178.729501432557,4.64240845069552,338.668238588125));
#23957=CARTESIAN_POINT('Ctrl Pts',(178.736899699983,4.54467945491274,338.791921359843));
#23958=CARTESIAN_POINT('Ctrl Pts',(178.744297967409,4.44202163202471,338.911674011555));
#23959=CARTESIAN_POINT('Ctrl Pts',(178.751696234834,4.33479509217015,339.027093501695));
#23960=CARTESIAN_POINT('Ctrl Pts',(178.759097101349,4.22753088250479,339.142553539916));
#23961=CARTESIAN_POINT('Ctrl Pts',(178.766497967864,4.11569501410163,339.253677112442));
#23962=CARTESIAN_POINT('Ctrl Pts',(178.773898834379,3.99968444984814,339.360098033777));
#23963=CARTESIAN_POINT('Ctrl Pts',(178.781307827753,3.88354649490353,339.466635815457));
#23964=CARTESIAN_POINT('Ctrl Pts',(178.788716821127,3.76322496437232,339.568460380802));
#23965=CARTESIAN_POINT('Ctrl Pts',(178.796125814501,3.63915045630747,339.665245386778));
#23966=CARTESIAN_POINT('Ctrl Pts',(178.80353937207,3.51499951406585,339.762090015657));
#23967=CARTESIAN_POINT('Ctrl Pts',(178.81095292964,3.38709128989435,339.853888681856));
#23968=CARTESIAN_POINT('Ctrl Pts',(178.818366487209,3.25588490340638,339.940358697329));
#23969=CARTESIAN_POINT('Ctrl Pts',(178.825790599335,3.12449172060499,340.0269518187));
#23970=CARTESIAN_POINT('Ctrl Pts',(178.833214711461,2.989791316273,340.108200945721));
#23971=CARTESIAN_POINT('Ctrl Pts',(178.840638823587,2.85226761727777,340.183869211499));
#23972=CARTESIAN_POINT('Ctrl Pts',(178.84449594887,2.78081851636686,340.223181923394));
#23973=CARTESIAN_POINT('Ctrl Pts',(178.848353074153,2.70860768957039,340.260989024843));
#23974=CARTESIAN_POINT('Ctrl Pts',(178.852210199437,2.6357049572448,340.297262494993));
#23975=CARTESIAN_POINT('Ctrl Pts',(178.859634176926,2.49538588437414,340.367079627202));
#23976=CARTESIAN_POINT('Ctrl Pts',(178.867058154416,2.35207914078279,340.431422868358));
#23977=CARTESIAN_POINT('Ctrl Pts',(178.874482131905,2.20625127720746,340.49002603494));
#23978=CARTESIAN_POINT('Ctrl Pts',(178.881897347984,2.06059551244881,340.54856004097));
#23979=CARTESIAN_POINT('Ctrl Pts',(178.889312564064,1.91242489301706,340.601367318671));
#23980=CARTESIAN_POINT('Ctrl Pts',(178.896727780143,1.76223046197014,340.648227541575));
#23981=CARTESIAN_POINT('Ctrl Pts',(178.904135861339,1.61218054724618,340.695042675809));
#23982=CARTESIAN_POINT('Ctrl Pts',(178.911543942534,1.46011105151351,340.735922036717));
#23983=CARTESIAN_POINT('Ctrl Pts',(178.91895202373,1.30653279142841,340.770693426913));
#23984=CARTESIAN_POINT('Ctrl Pts',(178.926354590956,1.15306884244633,340.805438936129));
#23985=CARTESIAN_POINT('Ctrl Pts',(178.933757158182,0.998098727609406,340.834085444868));
#23986=CARTESIAN_POINT('Ctrl Pts',(178.941159725407,0.842148109607813,340.856510661135));
#23987=CARTESIAN_POINT('Ctrl Pts',(178.948558395214,0.686279598925004,340.878924070623));
#23988=CARTESIAN_POINT('Ctrl Pts',(178.95595706502,0.529431981662636,340.895122657971));
#23989=CARTESIAN_POINT('Ctrl Pts',(178.963355734827,0.372140682503567,340.905035298364));
#23990=CARTESIAN_POINT('Ctrl Pts',(178.970753184082,0.214875331529375,340.914946303479));
#23991=CARTESIAN_POINT('Ctrl Pts',(178.978150633337,0.0571668160346099,
340.918573396271));
#23992=CARTESIAN_POINT('Ctrl Pts',(178.985548082593,-0.100444630773965,
340.915897348556));
#23993=CARTESIAN_POINT('Ctrl Pts',(178.992945211107,-0.258049243821911,
340.91322141687));
#23994=CARTESIAN_POINT('Ctrl Pts',(179.000342339622,-0.4155564233945,340.90424289441));
#23995=CARTESIAN_POINT('Ctrl Pts',(179.007739468137,-0.572426519144063,
340.888994688627));
#23996=CARTESIAN_POINT('Ctrl Pts',(179.015137735625,-0.729320768968311,
340.873744135002));
#23997=CARTESIAN_POINT('Ctrl Pts',(179.022536003112,-0.885577368166346,
340.852222011973));
#23998=CARTESIAN_POINT('Ctrl Pts',(179.0299342706,-1.04066251421858,340.824513034924));
#23999=CARTESIAN_POINT('Ctrl Pts',(179.037335137177,-1.1958021433088,340.79679432342));
#24000=CARTESIAN_POINT('Ctrl Pts',(179.044736003753,-1.34976913270849,340.762884496048));
#24001=CARTESIAN_POINT('Ctrl Pts',(179.05213687033,-1.50204072981682,340.722919203385));
#24002=CARTESIAN_POINT('Ctrl Pts',(179.059545863765,-1.65447953568255,340.682910025013));
#24003=CARTESIAN_POINT('Ctrl Pts',(179.0669548572,-1.80521887013696,340.636832196786));
#24004=CARTESIAN_POINT('Ctrl Pts',(179.074363850635,-1.95375128304053,340.584871214855));
#24005=CARTESIAN_POINT('Ctrl Pts',(179.081777408265,-2.10237519702791,340.532878223169));
#24006=CARTESIAN_POINT('Ctrl Pts',(179.089190965895,-2.24878913413984,340.474994992921));
#24007=CARTESIAN_POINT('Ctrl Pts',(179.096604523526,-2.39250691999123,340.411454628868));
#24008=CARTESIAN_POINT('Ctrl Pts',(179.104028635712,-2.53642931440393,340.347823803482));
#24009=CARTESIAN_POINT('Ctrl Pts',(179.111452747897,-2.67764755723836,340.278519922891));
#24010=CARTESIAN_POINT('Ctrl Pts',(179.118876860083,-2.81570058146565,340.203821749256));
#24011=CARTESIAN_POINT('Ctrl Pts',(179.122733984626,-2.88742467379915,340.165013047072));
#24012=CARTESIAN_POINT('Ctrl Pts',(179.126591109168,-2.95829488009628,340.124749021696));
#24013=CARTESIAN_POINT('Ctrl Pts',(179.130448233711,-3.0282498532578,340.083073222839));
#24014=CARTESIAN_POINT('Ctrl Pts',(179.13787221108,-3.1628952690151,340.002857978511));
#24015=CARTESIAN_POINT('Ctrl Pts',(179.14529618845,-3.29455437319437,339.917168101739));
#24016=CARTESIAN_POINT('Ctrl Pts',(179.15272016582,-3.42275084902876,339.826251877801));
#24017=CARTESIAN_POINT('Ctrl Pts',(179.160135381779,-3.55079603373473,339.735442948685));
#24018=CARTESIAN_POINT('Ctrl Pts',(179.167550597739,-3.67538642271923,339.639420163455));
#24019=CARTESIAN_POINT('Ctrl Pts',(179.174965813698,-3.79607100718653,339.538477219387));
#24020=CARTESIAN_POINT('Ctrl Pts',(179.182373894774,-3.91663946955667,339.43763140211));
#24021=CARTESIAN_POINT('Ctrl Pts',(179.189781975851,-4.03330932481586,339.331875088652));
#24022=CARTESIAN_POINT('Ctrl Pts',(179.197190056927,-4.1456593363124,339.22154464974));
#24023=CARTESIAN_POINT('Ctrl Pts',(179.204592624033,-4.25792572364706,339.111296331784));
#24024=CARTESIAN_POINT('Ctrl Pts',(179.21199519114,-4.36587840428412,338.996480927814));
#24025=CARTESIAN_POINT('Ctrl Pts',(179.219397758246,-4.46913007403816,338.87747429957));
#24026=CARTESIAN_POINT('Ctrl Pts',(179.226796427933,-4.57232738224324,338.758530327792));
#24027=CARTESIAN_POINT('Ctrl Pts',(179.234195097621,-4.67082836483336,338.635399807627));
#24028=CARTESIAN_POINT('Ctrl Pts',(179.241593767308,-4.76428346242158,338.508494499382));
#24029=CARTESIAN_POINT('Ctrl Pts',(179.248991216446,-4.85772314282943,338.381610126561));
#24030=CARTESIAN_POINT('Ctrl Pts',(179.256388665583,-4.94611836921755,338.250952501788));
#24031=CARTESIAN_POINT('Ctrl Pts',(179.26378611472,-5.02916062101619,338.116965513207));
#24032=CARTESIAN_POINT('Ctrl Pts',(179.271183243118,-5.11219927225257,337.98298433406));
#24033=CARTESIAN_POINT('Ctrl Pts',(179.278580371515,-5.18988521377237,337.845674395355));
#24034=CARTESIAN_POINT('Ctrl Pts',(179.285977499912,-5.26195408239006,337.70550730868));
#24035=CARTESIAN_POINT('Ctrl Pts',(179.293375767283,-5.33403404781942,337.565318639762));
#24036=CARTESIAN_POINT('Ctrl Pts',(179.300774034654,-5.40049504757217,337.422272278846));
#24037=CARTESIAN_POINT('Ctrl Pts',(179.308172302025,-5.46111944945291,337.276862956198));
#24038=CARTESIAN_POINT('Ctrl Pts',(179.315573168486,-5.52176514932835,337.131402549715));
#24039=CARTESIAN_POINT('Ctrl Pts',(179.322974034946,-5.57657002534469,336.98357787296));
#24040=CARTESIAN_POINT('Ctrl Pts',(179.330374901407,-5.6253652575456,336.833901928048));
#24041=CARTESIAN_POINT('Ctrl Pts',(179.337783894728,-5.67421407158467,336.684061624614));
#24042=CARTESIAN_POINT('Ctrl Pts',(179.345192888049,-5.71703994717826,336.532366348315));
#24043=CARTESIAN_POINT('Ctrl Pts',(179.35260188137,-5.75372426161535,336.379343207399));
#24044=CARTESIAN_POINT('Ctrl Pts',(179.360015438886,-5.79043117485847,336.226225798938));
#24045=CARTESIAN_POINT('Ctrl Pts',(179.367428996403,-5.8209889157249,336.071779261123));
#24046=CARTESIAN_POINT('Ctrl Pts',(179.37484255392,-5.84533041012745,335.916538574714));
#24047=CARTESIAN_POINT('Ctrl Pts',(179.382266665995,-5.86970655910858,335.761076874735));
#24048=CARTESIAN_POINT('Ctrl Pts',(179.38969077807,-5.88784874354698,335.604819137816));
#24049=CARTESIAN_POINT('Ctrl Pts',(179.397114890144,-5.89974187067178,335.448303939245));
#24050=CARTESIAN_POINT('Ctrl Pts',(179.400972016091,-5.90592083035877,335.366987974803));
#24051=CARTESIAN_POINT('Ctrl Pts',(179.404829142038,-5.91041388977135,335.285602502405));
#24052=CARTESIAN_POINT('Ctrl Pts',(179.408686267985,-5.91322447235937,335.204222677463));
#24053=CARTESIAN_POINT('Ctrl Pts',(179.411891385421,-5.91555995411032,335.136599296867));
#24054=CARTESIAN_POINT('Ctrl Pts',(179.415096502858,-5.9167354740858,335.068935624112));
#24055=CARTESIAN_POINT('Ctrl Pts',(179.418301620294,-5.91674986621234,335.001258243328));
#24056=CARTESIAN_POINT('',(181.168300457419,-5.91371740678573,335.004781946015));
#24057=CARTESIAN_POINT('Ctrl Pts',(179.418302920498,-5.92617389382204,335.001232749351));
#24058=CARTESIAN_POINT('Ctrl Pts',(179.507843381084,-5.92068436070428,333.107536126472));
#24059=CARTESIAN_POINT('Ctrl Pts',(179.690129853096,-3.91031427291091,329.242355225545));
#24060=CARTESIAN_POINT('Ctrl Pts',(179.965162336533,2.6771571405124,328.535833178706));
#24061=CARTESIAN_POINT('Ctrl Pts',(180.243400370805,6.88461919736723,333.753147063498));
#24062=CARTESIAN_POINT('Ctrl Pts',(180.52163840508,4.77416759640351,340.114679321284));
#24063=CARTESIAN_POINT('Ctrl Pts',(180.799876439354,-1.71746669328536,341.782546166841));
#24064=CARTESIAN_POINT('Ctrl Pts',(181.015430190788,-5.52558505666044,338.252676518138));
#24065=CARTESIAN_POINT('Ctrl Pts',(181.138237930799,-5.91644287689095,335.644616494525));
#24066=CARTESIAN_POINT('Ctrl Pts',(181.168299659384,-5.91163757001288,335.004797257822));
#24067=CARTESIAN_POINT('',(182.918301620326,-5.91674900113458,334.996561966701));
#24068=CARTESIAN_POINT('Ctrl Pts',(181.168301620294,-5.91674808559426,335.004759634086));
#24069=CARTESIAN_POINT('Ctrl Pts',(181.175682633724,-5.91687456571228,334.847530951683));
#24070=CARTESIAN_POINT('Ctrl Pts',(181.183063647155,-5.91072959315671,334.690217571805));
#24071=CARTESIAN_POINT('Ctrl Pts',(181.190444660585,-5.8983197483079,334.533358050299));
#24072=CARTESIAN_POINT('Ctrl Pts',(181.197824885786,-5.88591122872514,334.376515280057));
#24073=CARTESIAN_POINT('Ctrl Pts',(181.205205110986,-5.86723919029723,334.220126645509));
#24074=CARTESIAN_POINT('Ctrl Pts',(181.212585336187,-5.84236226494832,334.064727992717));
#24075=CARTESIAN_POINT('Ctrl Pts',(181.219965521659,-5.8174854735172,333.909330176468));
#24076=CARTESIAN_POINT('Ctrl Pts',(181.22734570713,-5.78640392014178,333.754922701516));
#24077=CARTESIAN_POINT('Ctrl Pts',(181.234725892601,-5.74922774037012,333.602033279417));
#24078=CARTESIAN_POINT('Ctrl Pts',(181.242107508479,-5.71204435521699,333.449114224724));
#24079=CARTESIAN_POINT('Ctrl Pts',(181.249489124357,-5.66876408028079,333.297714172808));
#24080=CARTESIAN_POINT('Ctrl Pts',(181.256870740235,-5.61954745989454,333.148347519513));
#24081=CARTESIAN_POINT('Ctrl Pts',(181.264255257255,-5.5703114962613,332.998922161739));
#24082=CARTESIAN_POINT('Ctrl Pts',(181.271639774276,-5.51513465925886,332.851532149276));
#24083=CARTESIAN_POINT('Ctrl Pts',(181.279024291296,-5.45422627296556,332.706673523941));
#24084=CARTESIAN_POINT('Ctrl Pts',(181.286417357171,-5.39324737468555,332.561647199705));
#24085=CARTESIAN_POINT('Ctrl Pts',(181.293810423046,-5.32652382228588,332.419158460163));
#24086=CARTESIAN_POINT('Ctrl Pts',(181.301203488922,-5.25431202131066,332.279680947901));
#24087=CARTESIAN_POINT('Ctrl Pts',(181.308601398843,-5.18205290609127,332.140112047903));
#24088=CARTESIAN_POINT('Ctrl Pts',(181.315999308765,-5.10429856273563,332.003558630727));
#24089=CARTESIAN_POINT('Ctrl Pts',(181.323397218687,-5.02134936621406,331.870466311905));
#24090=CARTESIAN_POINT('Ctrl Pts',(181.330805981087,-4.9382784860901,331.737178751254));
#24091=CARTESIAN_POINT('Ctrl Pts',(181.338214743487,-4.84999774448374,331.607362736975));
#24092=CARTESIAN_POINT('Ctrl Pts',(181.345623505886,-4.75684897720122,331.481432341051));
#24093=CARTESIAN_POINT('Ctrl Pts',(181.349199839891,-4.71188450324754,331.420643624542));
#24094=CARTESIAN_POINT('Ctrl Pts',(181.352776173896,-4.6657862783406,331.360759791651));
#24095=CARTESIAN_POINT('Ctrl Pts',(181.356352507901,-4.61859582054146,331.301824340438));
#24096=CARTESIAN_POINT('Ctrl Pts',(181.363776498333,-4.52063475016631,331.179482236693));
#24097=CARTESIAN_POINT('Ctrl Pts',(181.371200488764,-4.4176614625104,331.060850606176));
#24098=CARTESIAN_POINT('Ctrl Pts',(181.378624479195,-4.30998735794272,330.946367118636));
#24099=CARTESIAN_POINT('Ctrl Pts',(181.386039708267,-4.20244032405714,330.832018737814));
#24100=CARTESIAN_POINT('Ctrl Pts',(181.393454937339,-4.09020376910877,330.721809024822));
#24101=CARTESIAN_POINT('Ctrl Pts',(181.400870166411,-3.97363059578821,330.616144339658));
#24102=CARTESIAN_POINT('Ctrl Pts',(181.408278260637,-3.85716958779107,330.510581323799));
#24103=CARTESIAN_POINT('Ctrl Pts',(181.415686354864,-3.73638054304779,330.409554878568));
#24104=CARTESIAN_POINT('Ctrl Pts',(181.42309444909,-3.61165454041747,330.313436008846));
#24105=CARTESIAN_POINT('Ctrl Pts',(181.430497029372,-3.48702137303549,330.217388681697));
#24106=CARTESIAN_POINT('Ctrl Pts',(181.437899609654,-3.35845737682992,330.126241883687));
#24107=CARTESIAN_POINT('Ctrl Pts',(181.445302189936,-3.22638808277122,330.040327581195));
#24108=CARTESIAN_POINT('Ctrl Pts',(181.452700872812,-3.09438832226619,329.954458511979));
#24109=CARTESIAN_POINT('Ctrl Pts',(181.460099555687,-2.95888725141271,329.873816654786));
#24110=CARTESIAN_POINT('Ctrl Pts',(181.467498238563,-2.82034077094226,329.798691655145));
#24111=CARTESIAN_POINT('Ctrl Pts',(181.474895700865,-2.68181714672183,329.723579049003));
#24112=CARTESIAN_POINT('Ctrl Pts',(181.482293163167,-2.54024943776219,329.653981671833));
#24113=CARTESIAN_POINT('Ctrl Pts',(181.489690625469,-2.39611972686203,329.590144103856));
#24114=CARTESIAN_POINT('Ctrl Pts',(181.497087767015,-2.25199626546311,329.526309303893));
#24115=CARTESIAN_POINT('Ctrl Pts',(181.504484908562,-2.10531136424191,329.468233967683));
#24116=CARTESIAN_POINT('Ctrl Pts',(181.511882050108,-1.956568496847,329.416115126577));
#24117=CARTESIAN_POINT('Ctrl Pts',(181.519280330601,-1.80780272733961,329.363988260671));
#24118=CARTESIAN_POINT('Ctrl Pts',(181.526678611094,-1.65697871296884,329.317819839414));
#24119=CARTESIAN_POINT('Ctrl Pts',(181.534076891586,-1.50461640345109,329.277757429035));
#24120=CARTESIAN_POINT('Ctrl Pts',(181.54147777113,-1.35220056832682,329.23768094454));
#24121=CARTESIAN_POINT('Ctrl Pts',(181.548878650674,-1.1982457228128,329.203714836601));
#24122=CARTESIAN_POINT('Ctrl Pts',(181.556279530218,-1.04328320581177,329.175955811039));
#24123=CARTESIAN_POINT('Ctrl Pts',(181.563688536498,-0.888150528031741,
329.148166303929));
#24124=CARTESIAN_POINT('Ctrl Pts',(181.571097542778,-0.732008336604633,
329.126597556666));
#24125=CARTESIAN_POINT('Ctrl Pts',(181.578506549058,-0.575395043081121,
329.111294615376));
#24126=CARTESIAN_POINT('Ctrl Pts',(181.585920119482,-0.418685271604262,
329.095982247068));
#24127=CARTESIAN_POINT('Ctrl Pts',(181.593333689907,-0.261504191470108,
329.086943397476));
#24128=CARTESIAN_POINT('Ctrl Pts',(181.600747260332,-0.104390926711651,
329.084170971291));
#24129=CARTESIAN_POINT('Ctrl Pts',(181.608171385123,0.0529460131384107,
329.081394598127));
#24130=CARTESIAN_POINT('Ctrl Pts',(181.615595509915,0.210214572680946,329.084902457541));
#24131=CARTESIAN_POINT('Ctrl Pts',(181.623019634707,0.366879212260065,329.094635472207));
#24132=CARTESIAN_POINT('Ctrl Pts',(181.626876603863,0.448269369311689,329.099691952051));
#24133=CARTESIAN_POINT('Ctrl Pts',(181.630733573019,0.529496660050726,329.106427748144));
#24134=CARTESIAN_POINT('Ctrl Pts',(181.634590542176,0.610487122077327,329.114829141284));
#24135=CARTESIAN_POINT('Ctrl Pts',(181.642014491516,0.766378720569057,329.131000262838));
#24136=CARTESIAN_POINT('Ctrl Pts',(181.649438440856,0.921862522342883,329.153394149161));
#24137=CARTESIAN_POINT('Ctrl Pts',(181.656862390196,1.07640196975953,329.181985788777));
#24138=CARTESIAN_POINT('Ctrl Pts',(181.664277578124,1.23075903663928,329.210543685819));
#24139=CARTESIAN_POINT('Ctrl Pts',(181.671692766052,1.38417360414381,329.245284709667));
#24140=CARTESIAN_POINT('Ctrl Pts',(181.679107953979,1.53611298402458,329.286132005129));
#24141=CARTESIAN_POINT('Ctrl Pts',(181.686516007047,1.68790616853565,329.326939997512));
#24142=CARTESIAN_POINT('Ctrl Pts',(181.693924060115,1.83822663321251,329.373842468387));
#24143=CARTESIAN_POINT('Ctrl Pts',(181.701332113183,1.98655076106678,329.426711326676));
#24144=CARTESIAN_POINT('Ctrl Pts',(181.708734652331,2.13476448914581,329.479540833915));
#24145=CARTESIAN_POINT('Ctrl Pts',(181.716137191479,2.2809844890056,329.538327761386));
#24146=CARTESIAN_POINT('Ctrl Pts',(181.723539730627,2.4247013277235,329.602893920457));
#24147=CARTESIAN_POINT('Ctrl Pts',(181.730938372431,2.56834250134204,329.667426086262));
#24148=CARTESIAN_POINT('Ctrl Pts',(181.738337014236,2.70948279888093,329.737731271405));
#24149=CARTESIAN_POINT('Ctrl Pts',(181.745735656041,2.84763194093631,329.813582846371));
#24150=CARTESIAN_POINT('Ctrl Pts',(181.753133077496,2.98575829634621,329.889421910198));
#24151=CARTESIAN_POINT('Ctrl Pts',(181.760530498951,3.12089414861938,329.970805368751));
#24152=CARTESIAN_POINT('Ctrl Pts',(181.767927920406,3.25257294598057,330.057460187963));
#24153=CARTESIAN_POINT('Ctrl Pts',(181.775325021248,3.38424603622782,330.144111251452));
#24154=CARTESIAN_POINT('Ctrl Pts',(181.78272212209,3.51246205771631,330.236033016168));
#24155=CARTESIAN_POINT('Ctrl Pts',(181.790119222932,3.63678286766842,330.332908728562));
#24156=CARTESIAN_POINT('Ctrl Pts',(181.797517462899,3.76112282253035,330.42979935943));
#24157=CARTESIAN_POINT('Ctrl Pts',(181.804915702865,3.88156607707473,330.531645227573));
#24158=CARTESIAN_POINT('Ctrl Pts',(181.812313942831,3.99770716865451,330.638088955952));
#24159=CARTESIAN_POINT('Ctrl Pts',(181.819714782061,4.11388906471168,330.744570081781));
#24160=CARTESIAN_POINT('Ctrl Pts',(181.827115621291,4.22576551344088,330.855652032078));
#24161=CARTESIAN_POINT('Ctrl Pts',(181.834516460521,4.33296765850278,330.970940328952));
#24162=CARTESIAN_POINT('Ctrl Pts',(181.841925427011,4.44028752802186,331.086355230121));
#24163=CARTESIAN_POINT('Ctrl Pts',(181.849334393502,4.54292258849431,331.205985429211));
#24164=CARTESIAN_POINT('Ctrl Pts',(181.856743359993,4.64054359794924,331.329402544812));
#24165=CARTESIAN_POINT('Ctrl Pts',(181.864156890866,4.73822474800165,331.452895693012));
#24166=CARTESIAN_POINT('Ctrl Pts',(181.87157042174,4.83088547272313,331.580180105459));
#24167=CARTESIAN_POINT('Ctrl Pts',(181.878983952613,4.91823999153433,331.71079858504));
#24168=CARTESIAN_POINT('Ctrl Pts',(181.886408038565,5.00571888208932,331.8416030338));
#24169=CARTESIAN_POINT('Ctrl Pts',(181.893832124516,5.08787628398089,331.975750712805));
#24170=CARTESIAN_POINT('Ctrl Pts',(181.901256210468,5.16447206921048,332.112759308813));
#24171=CARTESIAN_POINT('Ctrl Pts',(181.905113665795,5.20427021024835,332.183947134762));
#24172=CARTESIAN_POINT('Ctrl Pts',(181.908971121122,5.24256766562074,332.255906973951));
#24173=CARTESIAN_POINT('Ctrl Pts',(181.91282857645,5.2793359363705,332.328569178615));
#24174=CARTESIAN_POINT('Ctrl Pts',(181.920252564985,5.35009948315099,332.468413539364));
#24175=CARTESIAN_POINT('Ctrl Pts',(181.92767655352,5.41540943627099,332.611282488728));
#24176=CARTESIAN_POINT('Ctrl Pts',(181.935100542055,5.47499646572596,332.756711284121));
#24177=CARTESIAN_POINT('Ctrl Pts',(181.942515769003,5.53451317220456,332.901968448443));
#24178=CARTESIAN_POINT('Ctrl Pts',(181.94993099595,5.58832025891396,333.049779103337));
#24179=CARTESIAN_POINT('Ctrl Pts',(181.957346222898,5.63619408637256,333.199653704634));
#24180=CARTESIAN_POINT('Ctrl Pts',(181.964754314777,5.68402184874883,333.349384093817));
#24181=CARTESIAN_POINT('Ctrl Pts',(181.972162406656,5.72592760481096,333.501174122574));
#24182=CARTESIAN_POINT('Ctrl Pts',(181.979570498535,5.76173570945806,333.6545141484));
#24183=CARTESIAN_POINT('Ctrl Pts',(181.986973076251,5.79751716058468,333.807740036615));
#24184=CARTESIAN_POINT('Ctrl Pts',(181.994375653968,5.82720991309449,333.96251326278));
#24185=CARTESIAN_POINT('Ctrl Pts',(182.001778231684,5.85068812582356,334.118309001494));
#24186=CARTESIAN_POINT('Ctrl Pts',(182.009176911779,5.87415397675598,334.274022710316));
#24187=CARTESIAN_POINT('Ctrl Pts',(182.016575591875,5.89141174899934,334.430757491367));
#24188=CARTESIAN_POINT('Ctrl Pts',(182.023974271971,5.90238670143731,334.587978411736));
#24189=CARTESIAN_POINT('Ctrl Pts',(182.031371731185,5.91335984286074,334.745173388541));
#24190=CARTESIAN_POINT('Ctrl Pts',(182.038769190399,5.91805219613118,334.902853973512));
#24191=CARTESIAN_POINT('Ctrl Pts',(182.046166649613,5.91644088308741,335.060480074669));
#24192=CARTESIAN_POINT('Ctrl Pts',(182.053563787881,5.91482963995212,335.218099337053));
#24193=CARTESIAN_POINT('Ctrl Pts',(182.060960926148,5.90691527810846,335.375663747132));
#24194=CARTESIAN_POINT('Ctrl Pts',(182.068358064416,5.89272705777317,335.532633443456));
#24195=CARTESIAN_POINT('Ctrl Pts',(182.075756341443,5.8785366532187,335.689627304631));
#24196=CARTESIAN_POINT('Ctrl Pts',(182.083154618471,5.85807050066655,335.846025898037));
#24197=CARTESIAN_POINT('Ctrl Pts',(182.090552895498,5.83140970659936,336.001294859808));
#24198=CARTESIAN_POINT('Ctrl Pts',(182.097953771393,5.80473954712484,336.156618364481));
#24199=CARTESIAN_POINT('Ctrl Pts',(182.105354647288,5.77187047673323,336.31081107986));
#24200=CARTESIAN_POINT('Ctrl Pts',(182.112755523183,5.73293461061827,336.463349347516));
#24201=CARTESIAN_POINT('Ctrl Pts',(182.120164525555,5.69395599126166,336.616055108695));
#24202=CARTESIAN_POINT('Ctrl Pts',(182.127573527927,5.64889736496822,336.767102432364));
#24203=CARTESIAN_POINT('Ctrl Pts',(182.1349825303,5.59794079477748,336.915982625356));
#24204=CARTESIAN_POINT('Ctrl Pts',(182.142396096665,5.54695283501408,337.064954529498));
#24205=CARTESIAN_POINT('Ctrl Pts',(182.14980966303,5.49005982632769,337.211756295688));
#24206=CARTESIAN_POINT('Ctrl Pts',(182.157223229395,5.42749158307523,337.35590018425));
#24207=CARTESIAN_POINT('Ctrl Pts',(182.164647349926,5.36483426587322,337.500249280194));
#24208=CARTESIAN_POINT('Ctrl Pts',(182.172071470458,5.29648573959151,337.641932606207));
#24209=CARTESIAN_POINT('Ctrl Pts',(182.179495590989,5.22272164463501,337.780487220823));
#24210=CARTESIAN_POINT('Ctrl Pts',(182.183352597567,5.18439944899157,337.852469627057));
#24211=CARTESIAN_POINT('Ctrl Pts',(182.187209604146,5.14461628326591,337.923608050044));
#24212=CARTESIAN_POINT('Ctrl Pts',(182.191066610724,5.10341527751716,337.99384085544));
#24213=CARTESIAN_POINT('Ctrl Pts',(182.198490665663,5.02411063438275,338.129026574018));
#24214=CARTESIAN_POINT('Ctrl Pts',(182.205914720603,4.93931120921902,338.261262938105));
#24215=CARTESIAN_POINT('Ctrl Pts',(182.213338775543,4.84926207516582,338.390071959245));
#24216=CARTESIAN_POINT('Ctrl Pts',(182.220754069442,4.75931920704098,338.518728974368));
#24217=CARTESIAN_POINT('Ctrl Pts',(182.228169363342,4.66413917326874,338.643966394428));
#24218=CARTESIAN_POINT('Ctrl Pts',(182.235584657241,4.56401262852332,338.765331232333));
#24219=CARTESIAN_POINT('Ctrl Pts',(182.24299281655,4.46398242007042,338.886579299619));
#24220=CARTESIAN_POINT('Ctrl Pts',(182.250400975859,4.35901541136668,339.003961916544));
#24221=CARTESIAN_POINT('Ctrl Pts',(182.257809135167,4.2494451302821,339.117055579807));
#24222=CARTESIAN_POINT('Ctrl Pts',(182.265211780722,4.13995640030056,339.23006506958));
#24223=CARTESIAN_POINT('Ctrl Pts',(182.272614426277,4.02587147843684,339.338791694916));
#24224=CARTESIAN_POINT('Ctrl Pts',(182.280017071832,3.90756361151544,339.442845617896));
#24225=CARTESIAN_POINT('Ctrl Pts',(182.287415820107,3.78931803026757,339.546844759493));
#24226=CARTESIAN_POINT('Ctrl Pts',(182.294814568383,3.66685421124456,339.646175852206));
#24227=CARTESIAN_POINT('Ctrl Pts',(182.302213316659,3.54058155364649,339.740486559888));
#24228=CARTESIAN_POINT('Ctrl Pts',(182.309610844342,3.41432972760946,339.834781708863));
#24229=CARTESIAN_POINT('Ctrl Pts',(182.317008372025,3.28427060879882,339.924057893467));
#24230=CARTESIAN_POINT('Ctrl Pts',(182.324405899708,3.15084600044121,340.008003598641));
#24231=CARTESIAN_POINT('Ctrl Pts',(182.331803106617,3.0174271776934,340.091945663729));
#24232=CARTESIAN_POINT('Ctrl Pts',(182.339200313526,2.88064347144987,340.170557510235));
#24233=CARTESIAN_POINT('Ctrl Pts',(182.346597520434,2.74096470582782,340.243571592332));
#24234=CARTESIAN_POINT('Ctrl Pts',(182.353995866214,2.60126443531217,340.316596915651));
#24235=CARTESIAN_POINT('Ctrl Pts',(182.361394211994,2.45866854868735,340.384022585646));
#24236=CARTESIAN_POINT('Ctrl Pts',(182.368792557775,2.31367030378293,340.445627630301));
#24237=CARTESIAN_POINT('Ctrl Pts',(182.376193502474,2.16862112333624,340.507254315812));
#24238=CARTESIAN_POINT('Ctrl Pts',(182.383594447173,2.02116824765639,340.56305615916));
#24239=CARTESIAN_POINT('Ctrl Pts',(182.390995391873,1.87182353572629,340.612860876024));
#24240=CARTESIAN_POINT('Ctrl Pts',(182.398404462779,1.72231484392265,340.66272027826));
#24241=CARTESIAN_POINT('Ctrl Pts',(182.405813533685,1.57091052177811,340.706569285638));
#24242=CARTESIAN_POINT('Ctrl Pts',(182.413222604591,1.41813687320069,340.744285714636));
#24243=CARTESIAN_POINT('Ctrl Pts',(182.420636239438,1.26526911701207,340.782025376718));
#24244=CARTESIAN_POINT('Ctrl Pts',(182.428049874286,1.11103071836581,340.813624858261));
#24245=CARTESIAN_POINT('Ctrl Pts',(182.435463509133,0.955956201956742,340.839013469966));
#24246=CARTESIAN_POINT('Ctrl Pts',(182.442887697474,0.800660933103974,340.864438222993));
#24247=CARTESIAN_POINT('Ctrl Pts',(182.450311885816,0.644527538766438,340.88363440286));
#24248=CARTESIAN_POINT('Ctrl Pts',(182.457736074157,0.488094489432406,340.896583276092));
#24249=CARTESIAN_POINT('Ctrl Pts',(182.461592264438,0.406841754914568,340.903309037454));
#24250=CARTESIAN_POINT('Ctrl Pts',(182.465448454718,0.325508170214552,340.908350223537));
#24251=CARTESIAN_POINT('Ctrl Pts',(182.469304644998,0.244168856578803,340.911709746933));
#24252=CARTESIAN_POINT('Ctrl Pts',(182.476728424502,0.0875777431645812,
340.918177363705));
#24253=CARTESIAN_POINT('Ctrl Pts',(182.484152204007,-0.0695068156684068,
340.918428695711));
#24254=CARTESIAN_POINT('Ctrl Pts',(182.491575983512,-0.226550281635667,
340.912411143721));
#24255=CARTESIAN_POINT('Ctrl Pts',(182.498991001481,-0.383408405106118,
340.906400693638));
#24256=CARTESIAN_POINT('Ctrl Pts',(182.506406019451,-0.540225162915335,
340.894136100585));
#24257=CARTESIAN_POINT('Ctrl Pts',(182.513821037421,-0.696462371684638,
340.875616625285));
#24258=CARTESIAN_POINT('Ctrl Pts',(182.521228920568,-0.852549247077918,
340.857114969653));
#24259=CARTESIAN_POINT('Ctrl Pts',(182.528636803716,-1.00805731544565,340.832370457163));
#24260=CARTESIAN_POINT('Ctrl Pts',(182.536044686863,-1.16244998371425,340.801434356938));
#24261=CARTESIAN_POINT('Ctrl Pts',(182.543447056287,-1.31672773676139,340.770521282605));
#24262=CARTESIAN_POINT('Ctrl Pts',(182.550849425711,-1.4698913783617,340.733425869595));
#24263=CARTESIAN_POINT('Ctrl Pts',(182.558251795135,-1.62141112949147,340.690251006033));
#24264=CARTESIAN_POINT('Ctrl Pts',(182.565650267569,-1.77285111280959,340.647098871946));
#24265=CARTESIAN_POINT('Ctrl Pts',(182.573048740004,-1.92264857116719,340.59787376338));
#24266=CARTESIAN_POINT('Ctrl Pts',(182.580447212439,-2.07028569619649,340.542729264417));
#24267=CARTESIAN_POINT('Ctrl Pts',(182.587844465587,-2.21789849027097,340.4875938534));
#24268=CARTESIAN_POINT('Ctrl Pts',(182.595241718736,-2.36335130831283,340.42654111855));
#24269=CARTESIAN_POINT('Ctrl Pts',(182.602638971884,-2.50614313261334,340.359773984167));
#24270=CARTESIAN_POINT('Ctrl Pts',(182.610035905096,-2.64892878104972,340.293009737518));
#24271=CARTESIAN_POINT('Ctrl Pts',(182.617432838307,-2.78905332648191,340.220531740842));
#24272=CARTESIAN_POINT('Ctrl Pts',(182.624829771518,-2.9260375617218,340.1425902763));
#24273=CARTESIAN_POINT('Ctrl Pts',(182.632227844672,-3.0630429076182,340.064636800189));
#24274=CARTESIAN_POINT('Ctrl Pts',(182.639625917825,-3.19690665528948,339.981218364317));
#24275=CARTESIAN_POINT('Ctrl Pts',(182.647023990979,-3.32717608107599,339.892630160559));
#24276=CARTESIAN_POINT('Ctrl Pts',(182.654424664357,-3.4574912930801,339.804010820419));
#24277=CARTESIAN_POINT('Ctrl Pts',(182.661825337735,-3.58420935952138,339.710218304431));
#24278=CARTESIAN_POINT('Ctrl Pts',(182.669226011114,-3.70690843339046,339.61158979409));
#24279=CARTESIAN_POINT('Ctrl Pts',(182.676634814044,-3.82974229073642,339.512852941501));
#24280=CARTESIAN_POINT('Ctrl Pts',(182.684043616974,-3.94854804781382,339.409269719623));
#24281=CARTESIAN_POINT('Ctrl Pts',(182.691452419904,-4.06293817176402,339.301216569172));
#24282=CARTESIAN_POINT('Ctrl Pts',(182.698865788272,-4.17739878495709,339.193096834435));
#24283=CARTESIAN_POINT('Ctrl Pts',(182.706279156639,-4.28743808283587,339.080501948831));
#24284=CARTESIAN_POINT('Ctrl Pts',(182.713692525006,-4.39270738723038,338.963843131693));
#24285=CARTESIAN_POINT('Ctrl Pts',(182.721116451491,-4.49812661614684,338.847018169092));
#24286=CARTESIAN_POINT('Ctrl Pts',(182.728540377976,-4.59876204562417,338.72611800155));
#24287=CARTESIAN_POINT('Ctrl Pts',(182.735964304461,-4.69430655360297,338.60158528197));
#24288=CARTESIAN_POINT('Ctrl Pts',(182.739823762731,-4.74397704027127,338.536844765549));
#24289=CARTESIAN_POINT('Ctrl Pts',(182.743683221002,-4.79227237015983,338.471122966409));
#24290=CARTESIAN_POINT('Ctrl Pts',(182.747542679272,-4.83915424449997,338.404484801029));
#24291=CARTESIAN_POINT('Ctrl Pts',(182.755048836972,-4.93033355450777,338.274882006239));
#24292=CARTESIAN_POINT('Ctrl Pts',(182.762554994673,-5.01643598000011,338.141424467438));
#24293=CARTESIAN_POINT('Ctrl Pts',(182.770061152373,-5.09712241388912,338.004542171501));
#24294=CARTESIAN_POINT('Ctrl Pts',(182.777558024154,-5.17770903003509,337.867829213596));
#24295=CARTESIAN_POINT('Ctrl Pts',(182.785054895935,-5.25289281146279,337.727700242247));
#24296=CARTESIAN_POINT('Ctrl Pts',(182.792551767716,-5.32237623071385,337.584616377963));
#24297=CARTESIAN_POINT('Ctrl Pts',(182.800040731471,-5.39178635583995,337.441683444746));
#24298=CARTESIAN_POINT('Ctrl Pts',(182.807529695227,-5.45550793449517,337.295802148505));
#24299=CARTESIAN_POINT('Ctrl Pts',(182.815018658982,-5.51328793537044,337.14746052448));
#24300=CARTESIAN_POINT('Ctrl Pts',(182.822501087381,-5.57101751365697,336.999248353009));
#24301=CARTESIAN_POINT('Ctrl Pts',(182.829983515779,-5.62281570936212,336.848580465654));
#24302=CARTESIAN_POINT('Ctrl Pts',(182.837465944177,-5.66847646330246,336.695967319109));
#24303=CARTESIAN_POINT('Ctrl Pts',(182.844942536867,-5.71410160542619,336.543473198881));
#24304=CARTESIAN_POINT('Ctrl Pts',(182.852419129556,-5.75359874162882,336.389037189035));
#24305=CARTESIAN_POINT('Ctrl Pts',(182.859895722245,-5.78681083456673,336.233187304282));
#24306=CARTESIAN_POINT('Ctrl Pts',(182.867368876273,-5.82000765247827,336.077409098573));
#24307=CARTESIAN_POINT('Ctrl Pts',(182.874842030301,-5.846925109297,335.920218666881));
#24308=CARTESIAN_POINT('Ctrl Pts',(182.882315184329,-5.86745664008178,335.762156899372));
#24309=CARTESIAN_POINT('Ctrl Pts',(182.889786702774,-5.88798367731465,335.604129725423));
#24310=CARTESIAN_POINT('Ctrl Pts',(182.89725822122,-5.90212752351781,335.445231954273));
#24311=CARTESIAN_POINT('Ctrl Pts',(182.904729739665,-5.90983311565753,335.286012425565));
#24312=CARTESIAN_POINT('Ctrl Pts',(182.909253699875,-5.91449880610392,335.189605943039));
#24313=CARTESIAN_POINT('Ctrl Pts',(182.913777660084,-5.9168050856102,335.093081634052));
#24314=CARTESIAN_POINT('Ctrl Pts',(182.918301620294,-5.91674900113497,334.996561967377));
#24315=CARTESIAN_POINT('Ctrl Pts',(182.918301620326,-5.91674900113458,334.996561966701));
#24316=CARTESIAN_POINT('Ctrl Pts',(182.926539808851,-5.91664687057866,334.820798437922));
#24317=CARTESIAN_POINT('Ctrl Pts',(182.934777997377,-5.90870884398697,334.645319786239));
#24318=CARTESIAN_POINT('Ctrl Pts',(182.943016185902,-5.89303513855422,334.470786037349));
#24319=CARTESIAN_POINT('Ctrl Pts',(182.951302560027,-5.87726975679178,334.295231431356));
#24320=CARTESIAN_POINT('Ctrl Pts',(182.959588934152,-5.85367802089785,334.120633019713));
#24321=CARTESIAN_POINT('Ctrl Pts',(182.967875308277,-5.82241199872577,333.947645934301));
#24322=CARTESIAN_POINT('Ctrl Pts',(182.976186416185,-5.79105265141491,333.774142504223));
#24323=CARTESIAN_POINT('Ctrl Pts',(182.984497524093,-5.75197324614276,333.602260224294));
#24324=CARTESIAN_POINT('Ctrl Pts',(182.992808632001,-5.70537596478024,333.432640544416));
#24325=CARTESIAN_POINT('Ctrl Pts',(183.001151291127,-5.65860178750894,333.262376942263));
#24326=CARTESIAN_POINT('Ctrl Pts',(183.009493950253,-5.60425265350634,333.094393338494));
#24327=CARTESIAN_POINT('Ctrl Pts',(183.017836609379,-5.54258047112392,332.929315986536));
#24328=CARTESIAN_POINT('Ctrl Pts',(183.020484644101,-5.52300516810979,332.876918956619));
#24329=CARTESIAN_POINT('Ctrl Pts',(183.023132678823,-5.50269242956288,332.824814546121));
#24330=CARTESIAN_POINT('Ctrl Pts',(183.025780713545,-5.48165127710042,332.773022263523));
#24331=CARTESIAN_POINT('Ctrl Pts',(183.033205134754,-5.42265719469586,332.627809771338));
#24332=CARTESIAN_POINT('Ctrl Pts',(183.040629555963,-5.35780005342511,332.484724222657));
#24333=CARTESIAN_POINT('Ctrl Pts',(183.048053977172,-5.28725352347771,332.344273971026));
#24334=CARTESIAN_POINT('Ctrl Pts',(183.055469639593,-5.21679021915741,332.20398941231));
#24335=CARTESIAN_POINT('Ctrl Pts',(183.062885302014,-5.14065105225165,332.066334292474));
#24336=CARTESIAN_POINT('Ctrl Pts',(183.070300964435,-5.0590584006965,331.931798790685));
#24337=CARTESIAN_POINT('Ctrl Pts',(183.077709494145,-4.97754422855538,331.79739269108));
#24338=CARTESIAN_POINT('Ctrl Pts',(183.085118023854,-4.89058720662411,331.666100552837));
#24339=CARTESIAN_POINT('Ctrl Pts',(183.092526553564,-4.79845638643319,331.538389555424));
#24340=CARTESIAN_POINT('Ctrl Pts',(183.09992957103,-4.70639411526576,331.410773580112));
#24341=CARTESIAN_POINT('Ctrl Pts',(183.107332588496,-4.6091659281835,331.286733741523));
#24342=CARTESIAN_POINT('Ctrl Pts',(183.114735605963,-4.50708503167518,331.16670962752));
#24343=CARTESIAN_POINT('Ctrl Pts',(183.122134727296,-4.40505785931685,331.046748681002));
#24344=CARTESIAN_POINT('Ctrl Pts',(183.129533848628,-4.29818330500363,330.930799533569));
#24345=CARTESIAN_POINT('Ctrl Pts',(183.136932969961,-4.18681575387772,330.819269871711));
#24346=CARTESIAN_POINT('Ctrl Pts',(183.144330871211,-4.07546656676774,330.707758600601));
#24347=CARTESIAN_POINT('Ctrl Pts',(183.151728772462,-3.95962611666547,330.60066563252));
#24348=CARTESIAN_POINT('Ctrl Pts',(183.159126673712,-3.83968673673909,330.498362928199));
#24349=CARTESIAN_POINT('Ctrl Pts',(183.166524254465,-3.71975255291265,330.39606465591));
#24350=CARTESIAN_POINT('Ctrl Pts',(183.173921835218,-3.59572007625608,330.298556476909));
#24351=CARTESIAN_POINT('Ctrl Pts',(183.181319415972,-3.46801570464513,330.206170879679));
#24352=CARTESIAN_POINT('Ctrl Pts',(183.188718135548,-3.34029167353395,330.113771060112));
#24353=CARTESIAN_POINT('Ctrl Pts',(183.196116855125,-3.20889492429432,330.026495611256));
#24354=CARTESIAN_POINT('Ctrl Pts',(183.203515574702,-3.07428175601834,329.944634311238));
#24355=CARTESIAN_POINT('Ctrl Pts',(183.210916892824,-2.9396213094921,329.86274426025));
#24356=CARTESIAN_POINT('Ctrl Pts',(183.218318210947,-2.80174251341328,329.786272337828));
#24357=CARTESIAN_POINT('Ctrl Pts',(183.22571952907,-2.66112709113199,329.715462823733));
#24358=CARTESIAN_POINT('Ctrl Pts',(183.233128970942,-2.52035732817522,329.644575588518));
#24359=CARTESIAN_POINT('Ctrl Pts',(183.240538412814,-2.37684527386209,329.579363341473));
#24360=CARTESIAN_POINT('Ctrl Pts',(183.247947854686,-2.23109416682969,329.520022866723));
#24361=CARTESIAN_POINT('Ctrl Pts',(183.255361859659,-2.0852532990533,329.460645847172));
#24362=CARTESIAN_POINT('Ctrl Pts',(183.262775864632,-1.93717098101059,329.407147932048));
#24363=CARTESIAN_POINT('Ctrl Pts',(183.270189869605,-1.7873660092298,329.359676134161));
#24364=CARTESIAN_POINT('Ctrl Pts',(183.277614423569,-1.63734788795967,329.31213679119));
#24365=CARTESIAN_POINT('Ctrl Pts',(183.285038977534,-1.48560257664327,329.270640788103));
#24366=CARTESIAN_POINT('Ctrl Pts',(183.292463531498,-1.33266026578227,329.235284293349));
#24367=CARTESIAN_POINT('Ctrl Pts',(183.296315270272,-1.25331626320317,329.21694191448));
#24368=CARTESIAN_POINT('Ctrl Pts',(183.300167009046,-1.1736502202182,329.200251052964));
#24369=CARTESIAN_POINT('Ctrl Pts',(183.30401874782,-1.09373663000128,329.185219630399));
#24370=CARTESIAN_POINT('Ctrl Pts',(183.311441361916,-0.939736637768514,
329.156252855763));
#24371=CARTESIAN_POINT('Ctrl Pts',(183.318863976013,-0.784352309190427,
329.133364376445));
#24372=CARTESIAN_POINT('Ctrl Pts',(183.32628659011,-0.628104860476675,329.116683346381));
#24373=CARTESIAN_POINT('Ctrl Pts',(183.333700441245,-0.47204187378618,329.100022009545));
#24374=CARTESIAN_POINT('Ctrl Pts',(183.341114292379,-0.315118162870769,
329.089553574084));
#24375=CARTESIAN_POINT('Ctrl Pts',(183.348528143514,-0.157866035844739,
329.085356403195));
#24376=CARTESIAN_POINT('Ctrl Pts',(183.355934859503,-0.000765249449437844,
329.081163271695));
#24377=CARTESIAN_POINT('Ctrl Pts',(183.363341575492,0.156662953096641,329.083229399167));
#24378=CARTESIAN_POINT('Ctrl Pts',(183.370748291481,0.313880332588857,329.091581455303));
#24379=CARTESIAN_POINT('Ctrl Pts',(183.378149494515,0.470980692309217,329.099927294852));
#24380=CARTESIAN_POINT('Ctrl Pts',(183.38555069755,0.627870170187996,329.114549727371));
#24381=CARTESIAN_POINT('Ctrl Pts',(183.392951900584,0.784009822882335,329.135423360538));
#24382=CARTESIAN_POINT('Ctrl Pts',(183.400349208488,0.940067301855593,329.156286008257));
#24383=CARTESIAN_POINT('Ctrl Pts',(183.407746516391,1.09537537241413,329.18339325528));
#24384=CARTESIAN_POINT('Ctrl Pts',(183.415143824295,1.24939962459685,329.216667816859));
#24385=CARTESIAN_POINT('Ctrl Pts',(183.422539919361,1.40339862349636,329.249936922855));
#24386=CARTESIAN_POINT('Ctrl Pts',(183.429936014428,1.55611385716661,329.289371257896));
#24387=CARTESIAN_POINT('Ctrl Pts',(183.437332109494,1.70702041513273,329.334842291267));
#24388=CARTESIAN_POINT('Ctrl Pts',(183.444727888732,1.85792052907156,329.380311382929));
#24389=CARTESIAN_POINT('Ctrl Pts',(183.45212366797,2.0070117633814,329.431816552673));
#24390=CARTESIAN_POINT('Ctrl Pts',(183.459519447208,2.1537839627113,329.489179262173));
#24391=CARTESIAN_POINT('Ctrl Pts',(183.466916371476,2.30057888562481,329.546550852689));
#24392=CARTESIAN_POINT('Ctrl Pts',(183.474313295744,2.44505371090248,329.609781652746));
#24393=CARTESIAN_POINT('Ctrl Pts',(183.481710220012,2.5867180170615,329.678644865947));
#24394=CARTESIAN_POINT('Ctrl Pts',(183.489109750576,2.72843223845886,329.747532343014));
#24395=CARTESIAN_POINT('Ctrl Pts',(183.496509281141,2.86733363352001,329.822056021361));
#24396=CARTESIAN_POINT('Ctrl Pts',(183.503908811706,3.00295628429228,329.901943103777));
#24397=CARTESIAN_POINT('Ctrl Pts',(183.511316486777,3.13872821204158,329.981918116211));
#24398=CARTESIAN_POINT('Ctrl Pts',(183.518724161849,3.27121386656859,330.067268132464));
#24399=CARTESIAN_POINT('Ctrl Pts',(183.52613183692,3.39997562864591,330.15767656108));
#24400=CARTESIAN_POINT('Ctrl Pts',(183.533544084214,3.52881686606072,330.248140792291));
#24401=CARTESIAN_POINT('Ctrl Pts',(183.540956331509,3.65392933497888,330.343669431135));
#24402=CARTESIAN_POINT('Ctrl Pts',(183.548368578803,3.77490885653954,330.443905873742));
#24403=CARTESIAN_POINT('Ctrl Pts',(183.555791404439,3.89606103325496,330.544285368151));
#24404=CARTESIAN_POINT('Ctrl Pts',(183.563214230074,4.01306820552597,330.649385836092));
#24405=CARTESIAN_POINT('Ctrl Pts',(183.57063705571,4.12556278929575,330.758813581782));
#24406=CARTESIAN_POINT('Ctrl Pts',(183.574510297838,4.18426264059047,330.815913152128));
#24407=CARTESIAN_POINT('Ctrl Pts',(183.578383539966,4.24173447469739,330.874190378549));
#24408=CARTESIAN_POINT('Ctrl Pts',(183.582256782094,4.29793053209515,330.933585891257));
#24409=CARTESIAN_POINT('Ctrl Pts',(183.589681965407,4.40566095892533,331.04744982108));
#24410=CARTESIAN_POINT('Ctrl Pts',(183.59710714872,4.50902576428197,331.165769412846));
#24411=CARTESIAN_POINT('Ctrl Pts',(183.604532332033,4.60763417503468,331.288175937419));
#24412=CARTESIAN_POINT('Ctrl Pts',(183.611948747775,4.70612615011179,331.410437925779));
#24413=CARTESIAN_POINT('Ctrl Pts',(183.619365163517,4.7998726781938,331.53677695334));
#24414=CARTESIAN_POINT('Ctrl Pts',(183.626781579259,4.88851970687147,331.666787489819));
#24415=CARTESIAN_POINT('Ctrl Pts',(183.634190852915,4.97708136753446,331.796672824793));
#24416=CARTESIAN_POINT('Ctrl Pts',(183.641600126571,5.06055309669955,331.930222323533));
#24417=CARTESIAN_POINT('Ctrl Pts',(183.649009400228,5.13862111105372,332.066997504343));
#24418=CARTESIAN_POINT('Ctrl Pts',(183.656413151672,5.21663094047282,332.203670745131));
#24419=CARTESIAN_POINT('Ctrl Pts',(183.663816903116,5.28924489020512,332.343564558347));
#24420=CARTESIAN_POINT('Ctrl Pts',(183.671220654561,5.35619258140474,332.486211704736));
#24421=CARTESIAN_POINT('Ctrl Pts',(183.678620499305,5.42310494664703,332.628783581211));
#24422=CARTESIAN_POINT('Ctrl Pts',(183.686020344048,5.48435684981207,332.774105560543));
#24423=CARTESIAN_POINT('Ctrl Pts',(183.693420188792,5.53972400567662,332.921686139336));
#24424=CARTESIAN_POINT('Ctrl Pts',(183.700818795492,5.59508189824538,333.069242026909));
#24425=CARTESIAN_POINT('Ctrl Pts',(183.708217402192,5.64455686679045,333.219055414939));
#24426=CARTESIAN_POINT('Ctrl Pts',(183.715616008892,5.68797286237348,333.370615061011));
#24427=CARTESIAN_POINT('Ctrl Pts',(183.723014283895,5.73138691151746,333.522167912316));
#24428=CARTESIAN_POINT('Ctrl Pts',(183.730412558898,5.76874242509563,333.675466507332));
#24429=CARTESIAN_POINT('Ctrl Pts',(183.737810833902,5.79991339090287,333.82998494859));
#24430=CARTESIAN_POINT('Ctrl Pts',(183.74521023597,5.8310891053442,333.984526929432));
#24431=CARTESIAN_POINT('Ctrl Pts',(183.752609638039,5.85607832225718,334.140288760794));
#24432=CARTESIAN_POINT('Ctrl Pts',(183.760009040107,5.87480628874774,334.296735019932));
#24433=CARTESIAN_POINT('Ctrl Pts',(183.767411028395,5.89354080098971,334.45323595977));
#24434=CARTESIAN_POINT('Ctrl Pts',(183.774813016684,5.90600966134355,334.61042143346));
#24435=CARTESIAN_POINT('Ctrl Pts',(183.782215004973,5.91219005950291,334.76775172161));
#24436=CARTESIAN_POINT('Ctrl Pts',(183.789625095016,5.91837722234083,334.925254213687));
#24437=CARTESIAN_POINT('Ctrl Pts',(183.79703518506,5.91826216267396,335.082901463745));
#24438=CARTESIAN_POINT('Ctrl Pts',(183.804445275103,5.91187421168256,335.240153841824));
#24439=CARTESIAN_POINT('Ctrl Pts',(183.811859916752,5.90548233692874,335.397502811278));
#24440=CARTESIAN_POINT('Ctrl Pts',(183.819274558401,5.89280992294359,335.554456054423));
#24441=CARTESIAN_POINT('Ctrl Pts',(183.82668920005,5.87393804654573,335.7104803923));
#24442=CARTESIAN_POINT('Ctrl Pts',(183.834114367373,5.85503938001932,335.866726219126));
#24443=CARTESIAN_POINT('Ctrl Pts',(183.841539534695,5.82992373382684,336.022040139743));
#24444=CARTESIAN_POINT('Ctrl Pts',(183.848964702017,5.79872318251752,336.175899661975));
#24445=CARTESIAN_POINT('Ctrl Pts',(183.852808073467,5.78257333660411,336.255539523199));
#24446=CARTESIAN_POINT('Ctrl Pts',(183.856651444917,5.76479401531116,336.334789961192));
#24447=CARTESIAN_POINT('Ctrl Pts',(183.860494816368,5.745408700489,336.413580357406));
#24448=CARTESIAN_POINT('Ctrl Pts',(183.86792119583,5.70795129994161,336.565823612539));
#24449=CARTESIAN_POINT('Ctrl Pts',(183.875347575292,5.66438224827763,336.71680545197));
#24450=CARTESIAN_POINT('Ctrl Pts',(183.882773954755,5.61480040370371,336.865997585494));
#24451=CARTESIAN_POINT('Ctrl Pts',(183.890191591026,5.5652769326017,337.015014072813));
#24452=CARTESIAN_POINT('Ctrl Pts',(183.897609227296,5.50975487603878,337.162244697913));
#24453=CARTESIAN_POINT('Ctrl Pts',(183.905026863567,5.44838390601436,337.307172159849));
#24454=CARTESIAN_POINT('Ctrl Pts',(183.912437380672,5.3870718375205,337.451960525902));
#24455=CARTESIAN_POINT('Ctrl Pts',(183.919847897777,5.31992217573912,337.59444978839));
#24456=CARTESIAN_POINT('Ctrl Pts',(183.927258414882,5.24713408733631,337.734138700215));
#24457=CARTESIAN_POINT('Ctrl Pts',(183.934663431263,5.17440002851701,337.873723922907));
#24458=CARTESIAN_POINT('Ctrl Pts',(183.942068447645,5.09603604838222,338.01051260459));
#24459=CARTESIAN_POINT('Ctrl Pts',(183.949473464026,5.01228897675539,338.144024455375));
#24460=CARTESIAN_POINT('Ctrl Pts',(183.956874593786,4.92858586089307,338.277466230689));
#24461=CARTESIAN_POINT('Ctrl Pts',(183.964275723546,4.83950547821191,338.407634285279));
#24462=CARTESIAN_POINT('Ctrl Pts',(183.971676853306,4.74533999730428,338.534073976657));
#24463=CARTESIAN_POINT('Ctrl Pts',(183.979076770668,4.65118994188332,338.660492955628));
#24464=CARTESIAN_POINT('Ctrl Pts',(183.98647668803,4.55195666401408,338.783184484726));
#24465=CARTESIAN_POINT('Ctrl Pts',(183.993876605392,4.44797502577763,338.901723815515));
#24466=CARTESIAN_POINT('Ctrl Pts',(184.001276206797,4.34399782728575,339.020258084984));
#24467=CARTESIAN_POINT('Ctrl Pts',(184.008675808202,4.23527291747377,339.1346402283));
#24468=CARTESIAN_POINT('Ctrl Pts',(184.016075409607,4.12217454982721,339.244479655182));
#24469=CARTESIAN_POINT('Ctrl Pts',(184.023476152596,4.00905873375754,339.35433602771));
#24470=CARTESIAN_POINT('Ctrl Pts',(184.030876895586,3.89156838392223,339.4596480285));
#24471=CARTESIAN_POINT('Ctrl Pts',(184.038277638576,3.77011349337935,339.560063026926));
#24472=CARTESIAN_POINT('Ctrl Pts',(184.045680981094,3.64861594152358,339.660513296354));
#24473=CARTESIAN_POINT('Ctrl Pts',(184.053084323611,3.52315136358953,339.75606290121));
#24474=CARTESIAN_POINT('Ctrl Pts',(184.060487666129,3.39416146581732,339.846400572225));
#24475=CARTESIAN_POINT('Ctrl Pts',(184.0678991236,3.26503017962389,339.936837264177));
#24476=CARTESIAN_POINT('Ctrl Pts',(184.07531058107,3.1323661622583,340.022050399218));
#24477=CARTESIAN_POINT('Ctrl Pts',(184.082722038541,2.99663925388541,340.101772608082));
#24478=CARTESIAN_POINT('Ctrl Pts',(184.090138057114,2.86082881748993,340.181543878982));
#24479=CARTESIAN_POINT('Ctrl Pts',(184.097554075688,2.72195206212223,340.255817314652));
#24480=CARTESIAN_POINT('Ctrl Pts',(184.104970094261,2.58050139879679,340.324372553955));
#24481=CARTESIAN_POINT('Ctrl Pts',(184.112396641331,2.43884991844474,340.393025120898));
#24482=CARTESIAN_POINT('Ctrl Pts',(184.1198231884,2.29461757291683,340.455943129235));
#24483=CARTESIAN_POINT('Ctrl Pts',(184.12724973547,2.14831537803079,340.512954888172));
#24484=CARTESIAN_POINT('Ctrl Pts',(184.131077440527,2.07290999165573,340.542339230039));
#24485=CARTESIAN_POINT('Ctrl Pts',(184.134905145584,1.99695499345246,340.570155418434));
#24486=CARTESIAN_POINT('Ctrl Pts',(184.138732850641,1.92052157876961,340.596385210829));
#24487=CARTESIAN_POINT('Ctrl Pts',(184.146147643844,1.77245950104464,340.647195940354));
#24488=CARTESIAN_POINT('Ctrl Pts',(184.153562437047,1.6221530117845,340.692204502841));
#24489=CARTESIAN_POINT('Ctrl Pts',(184.16097723025,1.47009814711048,340.731207726157));
#24490=CARTESIAN_POINT('Ctrl Pts',(184.168383247424,1.31822325210573,340.770164785892));
#24491=CARTESIAN_POINT('Ctrl Pts',(184.175789264598,1.16460445945112,340.803130561944));
#24492=CARTESIAN_POINT('Ctrl Pts',(184.183195281773,1.0097561678994,340.829950518134));
#24493=CARTESIAN_POINT('Ctrl Pts',(184.190594158053,0.855057181322792,340.856744614478));
#24494=CARTESIAN_POINT('Ctrl Pts',(184.197993034333,0.699131422039454,340.877404624149));
#24495=CARTESIAN_POINT('Ctrl Pts',(184.205391910613,0.542506666056472,340.891826294095));
#24496=CARTESIAN_POINT('Ctrl Pts',(184.212785275444,0.385998580423634,340.906237221286));
#24497=CARTESIAN_POINT('Ctrl Pts',(184.220178640274,0.228792905828073,340.914419026937));
#24498=CARTESIAN_POINT('Ctrl Pts',(184.227572005105,0.0714256663736467,
340.916318867056));
#24499=CARTESIAN_POINT('Ctrl Pts',(184.234961483519,-0.0858588509889629,
340.9182177085));
#24500=CARTESIAN_POINT('Ctrl Pts',(184.242350961933,-0.243304390835582,
340.913841156131));
#24501=CARTESIAN_POINT('Ctrl Pts',(184.249740440347,-0.400371899099182,
340.903188367731));
#24502=CARTESIAN_POINT('Ctrl Pts',(184.257128743439,-0.557414425237863,
340.892537273693));
#24503=CARTESIAN_POINT('Ctrl Pts',(184.264517046532,-0.714078666085097,
340.875611949497));
#24504=CARTESIAN_POINT('Ctrl Pts',(184.271905349624,-0.869827551905739,
340.85246363444));
#24505=CARTESIAN_POINT('Ctrl Pts',(184.279293360726,-1.02557028243996,340.829316234219));
#24506=CARTESIAN_POINT('Ctrl Pts',(184.286681371828,-1.18039735969538,340.799946387029));
#24507=CARTESIAN_POINT('Ctrl Pts',(184.294069382931,-1.3337790936864,340.76445694682));
#24508=CARTESIAN_POINT('Ctrl Pts',(184.301458569383,-1.48718522899295,340.728961860639));
#24509=CARTESIAN_POINT('Ctrl Pts',(184.308847755835,-1.63914519859986,340.687345327382));
#24510=CARTESIAN_POINT('Ctrl Pts',(184.316236942287,-1.78914188283228,340.639760800388));
#24511=CARTESIAN_POINT('Ctrl Pts',(184.323628771864,-1.93919222114951,340.592159252323));
#24512=CARTESIAN_POINT('Ctrl Pts',(184.331020601442,-2.08727751945924,340.538585573466));
#24513=CARTESIAN_POINT('Ctrl Pts',(184.338412431019,-2.23289828462096,340.479242266321));
#24514=CARTESIAN_POINT('Ctrl Pts',(184.345812499641,-2.37868136087638,340.419832814233));
#24515=CARTESIAN_POINT('Ctrl Pts',(184.353212568262,-2.521994071378,340.354641032428));
#24516=CARTESIAN_POINT('Ctrl Pts',(184.360612636884,-2.66235862400008,340.283916835049));
#24517=CARTESIAN_POINT('Ctrl Pts',(184.368017319712,-2.80281069890818,340.21314853862));
#24518=CARTESIAN_POINT('Ctrl Pts',(184.375422002539,-2.94031062676973,340.136841134336));
#24519=CARTESIAN_POINT('Ctrl Pts',(184.382826685367,-3.07440796947533,340.055288933357));
#24520=CARTESIAN_POINT('Ctrl Pts',(184.390242077437,-3.20869925445112,339.973618785082));
#24521=CARTESIAN_POINT('Ctrl Pts',(184.397657469507,-3.33957781514952,339.886688897118));
#24522=CARTESIAN_POINT('Ctrl Pts',(184.405072861577,-3.46662410392826,339.794835543015));
#24523=CARTESIAN_POINT('Ctrl Pts',(184.409038869357,-3.53457284687054,339.74570919697));
#24524=CARTESIAN_POINT('Ctrl Pts',(184.413004877136,-3.60142596182236,339.695175174371));
#24525=CARTESIAN_POINT('Ctrl Pts',(184.416970884915,-3.66712353095129,339.643289305142));
#24526=CARTESIAN_POINT('Ctrl Pts',(184.424315854089,-3.78879414960982,339.547197685734));
#24527=CARTESIAN_POINT('Ctrl Pts',(184.431660823263,-3.90688829422341,339.446159993294));
#24528=CARTESIAN_POINT('Ctrl Pts',(184.439005792438,-4.02097117590753,339.340474785668));
#24529=CARTESIAN_POINT('Ctrl Pts',(184.446342029751,-4.13491843334505,339.234915218949));
#24530=CARTESIAN_POINT('Ctrl Pts',(184.453678267064,-4.24486363906911,339.124719387582));
#24531=CARTESIAN_POINT('Ctrl Pts',(184.461014504377,-4.35040260922375,339.010227886313));
#24532=CARTESIAN_POINT('Ctrl Pts',(184.468343705105,-4.45584035120531,338.895846200077));
#24533=CARTESIAN_POINT('Ctrl Pts',(184.475672905833,-4.55688001118919,338.77717732259));
#24534=CARTESIAN_POINT('Ctrl Pts',(184.483002106562,-4.65315220035627,338.654600547641));
#24535=CARTESIAN_POINT('Ctrl Pts',(184.490325959316,-4.74935414159845,338.532113214557));
#24536=CARTESIAN_POINT('Ctrl Pts',(184.497649812071,-4.84079530148923,338.4057239592));
#24537=CARTESIAN_POINT('Ctrl Pts',(184.504973664825,-4.92714490377433,338.275847014088));
#24538=CARTESIAN_POINT('Ctrl Pts',(184.512294282053,-5.01345635858973,338.146027445927));
#24539=CARTESIAN_POINT('Ctrl Pts',(184.519614899281,-5.09468052050149,338.012723571383));
#24540=CARTESIAN_POINT('Ctrl Pts',(184.526935516509,-5.17052857858857,337.876380499951));
#24541=CARTESIAN_POINT('Ctrl Pts',(184.53425459916,-5.24636073710885,337.740066009288));
#24542=CARTESIAN_POINT('Ctrl Pts',(184.541573681811,-5.31681884834582,337.600713922922));
#24543=CARTESIAN_POINT('Ctrl Pts',(184.548892764463,-5.38165903229536,337.458795766755));
#24544=CARTESIAN_POINT('Ctrl Pts',(184.556211832807,-5.44649908949729,337.316877888006));
#24545=CARTESIAN_POINT('Ctrl Pts',(184.563530901151,-5.50572108288589,337.172394297112));
#24546=CARTESIAN_POINT('Ctrl Pts',(184.570849969495,-5.55912855969106,337.025838152303));
#24547=CARTESIAN_POINT('Ctrl Pts',(184.578170543571,-5.61254702386355,336.879251856918));
#24548=CARTESIAN_POINT('Ctrl Pts',(184.585491117646,-5.66014846107913,336.730592518268));
#24549=CARTESIAN_POINT('Ctrl Pts',(184.592811691721,-5.70178581912152,336.5803699046));
#24550=CARTESIAN_POINT('Ctrl Pts',(184.600138780446,-5.74346023065446,336.430013606364));
#24551=CARTESIAN_POINT('Ctrl Pts',(184.607465869172,-5.7791598637499,336.278091623847));
#24552=CARTESIAN_POINT('Ctrl Pts',(184.614792957897,-5.80878836913647,336.125125879662));
#24553=CARTESIAN_POINT('Ctrl Pts',(184.622123775781,-5.83843195410075,335.972082282787));
#24554=CARTESIAN_POINT('Ctrl Pts',(184.629454593666,-5.8619981987883,335.817994243005));
#24555=CARTESIAN_POINT('Ctrl Pts',(184.63678541155,-5.87944255883285,335.663389598867));
#24556=CARTESIAN_POINT('Ctrl Pts',(184.644125337449,-5.89690859224144,335.508592869567));
#24557=CARTESIAN_POINT('Ctrl Pts',(184.651465263347,-5.90823752770803,335.353278634368));
#24558=CARTESIAN_POINT('Ctrl Pts',(184.658805189246,-5.91343690518207,335.197976086765));
#24559=CARTESIAN_POINT('Ctrl Pts',(184.661970666252,-5.91567923161252,335.130999028657));
#24560=CARTESIAN_POINT('Ctrl Pts',(184.665136143258,-5.91678216518749,335.064024102548));
#24561=CARTESIAN_POINT('Ctrl Pts',(184.668301620265,-5.91674928609117,334.997093448832));
#24562=CARTESIAN_POINT('Origin',(188.466817376509,0.,335.));
#24563=CARTESIAN_POINT('',(5.59181737646044,-4.91824899013927,335.003151744596));
#24564=CARTESIAN_POINT('',(5.23193167942401,-1.34848449270165,339.730361626982));
#24565=CARTESIAN_POINT('Ctrl Pts',(5.59181737646048,-4.91824899013927,335.003151744596));
#24566=CARTESIAN_POINT('Ctrl Pts',(5.58294884481862,-4.91814826821296,335.160326762204));
#24567=CARTESIAN_POINT('Ctrl Pts',(5.57408031317672,-4.9105091665031,335.317206178995));
#24568=CARTESIAN_POINT('Ctrl Pts',(5.56521178153488,-4.89544054547172,335.47312252985));
#24569=CARTESIAN_POINT('Ctrl Pts',(5.55630199600642,-4.88030182950141,335.62976415922));
#24570=CARTESIAN_POINT('Ctrl Pts',(5.54739221047797,-4.85766442287388,335.785433593565));
#24571=CARTESIAN_POINT('Ctrl Pts',(5.53848242494951,-4.82768834052904,335.939472378104));
#24572=CARTESIAN_POINT('Ctrl Pts',(5.5295184298106,-4.79752987537137,336.094448377402));
#24573=CARTESIAN_POINT('Ctrl Pts',(5.52055443467166,-4.75994324974078,336.247773676907));
#24574=CARTESIAN_POINT('Ctrl Pts',(5.51159043953274,-4.71514005962174,336.398798513243));
#24575=CARTESIAN_POINT('Ctrl Pts',(5.50436251686681,-4.67901398097615,336.520574107802));
#24576=CARTESIAN_POINT('Ctrl Pts',(5.49713459420093,-4.63819689184413,336.640854391806));
#24577=CARTESIAN_POINT('Ctrl Pts',(5.48990667153501,-4.59282194495883,336.759309422587));
#24578=CARTESIAN_POINT('Ctrl Pts',(5.48227368227759,-4.54490409938414,336.884402899542));
#24579=CARTESIAN_POINT('Ctrl Pts',(5.47464069302027,-4.49178076133987,337.007774141784));
#24580=CARTESIAN_POINT('Ctrl Pts',(5.46700770376285,-4.43359543719221,337.128946819864));
#24581=CARTESIAN_POINT('Ctrl Pts',(5.45938429306256,-4.37548312918977,337.249967439637));
#24582=CARTESIAN_POINT('Ctrl Pts',(5.4517608823622,-4.31232163831185,337.368794618869));
#24583=CARTESIAN_POINT('Ctrl Pts',(5.44413747166192,-4.24430379017305,337.484968490589));
#24584=CARTESIAN_POINT('Ctrl Pts',(5.43652165353137,-4.17635368471205,337.601026658427));
#24585=CARTESIAN_POINT('Ctrl Pts',(5.4289058354008,-4.1035570438768,337.714436426043));
#24586=CARTESIAN_POINT('Ctrl Pts',(5.42129001727025,-4.02615396193197,337.8247596955));
#24587=CARTESIAN_POINT('Ctrl Pts',(5.41339890657748,-3.94595295435561,337.9390708721));
#24588=CARTESIAN_POINT('Ctrl Pts',(5.40550779588471,-3.86080638509852,338.050067802952));
#24589=CARTESIAN_POINT('Ctrl Pts',(5.39761668519193,-3.77103258556973,338.157292558676));
#24590=CARTESIAN_POINT('Ctrl Pts',(5.39000943705944,-3.68448816927644,338.26066017757));
#24591=CARTESIAN_POINT('Ctrl Pts',(5.38240218892692,-3.59364395540761,338.360521977631));
#24592=CARTESIAN_POINT('Ctrl Pts',(5.37479494079443,-3.49882770338158,338.456499351157));
#24593=CARTESIAN_POINT('Ctrl Pts',(5.36718883430481,-3.40402568071896,338.552462321067));
#24594=CARTESIAN_POINT('Ctrl Pts',(5.3595827278152,-3.30525309005061,338.644541734526));
#24595=CARTESIAN_POINT('Ctrl Pts',(5.35197662132558,-3.20287540405726,338.732394969532));
#24596=CARTESIAN_POINT('Ctrl Pts',(5.34436987818154,-3.10048914873791,338.820255558122));
#24597=CARTESIAN_POINT('Ctrl Pts',(5.33676313503756,-2.99449750653069,338.903889000905));
#24598=CARTESIAN_POINT('Ctrl Pts',(5.32915639189352,-2.8852994839743,338.982992587274));
#24599=CARTESIAN_POINT('Ctrl Pts',(5.32154723335298,-2.77606678737726,339.062121291689));
#24600=CARTESIAN_POINT('Ctrl Pts',(5.31393807481246,-2.66362601507148,339.136717042431));
#24601=CARTESIAN_POINT('Ctrl Pts',(5.30632891627192,-2.54840511175222,339.206520468142));
#24602=CARTESIAN_POINT('Ctrl Pts',(5.29871147467145,-2.4330587830468,339.276399879385));
#24603=CARTESIAN_POINT('Ctrl Pts',(5.29109403307089,-2.31492663129186,339.341476344963));
#24604=CARTESIAN_POINT('Ctrl Pts',(5.28347659147042,-2.19446132130872,339.401536387647));
#24605=CARTESIAN_POINT('Ctrl Pts',(5.27585421093814,-2.07391790505556,339.461635371549));
#24606=CARTESIAN_POINT('Ctrl Pts',(5.26823183040589,-1.95103868932618,339.51671129508));
#24607=CARTESIAN_POINT('Ctrl Pts',(5.26060944987361,-1.82629492513081,339.566599381262));
#24608=CARTESIAN_POINT('Ctrl Pts',(5.25297632621633,-1.70137534475228,339.616557780641));
#24609=CARTESIAN_POINT('Ctrl Pts',(5.24534320255909,-1.57458635373703,339.661313621609));
#24610=CARTESIAN_POINT('Ctrl Pts',(5.23771007890181,-1.44641306659626,339.700752312479));
#24611=CARTESIAN_POINT('Ctrl Pts',(5.23577450614907,-1.41391146785913,339.710752996194));
#24612=CARTESIAN_POINT('Ctrl Pts',(5.23383893339626,-1.38132090062803,339.72041204255));
#24613=CARTESIAN_POINT('Ctrl Pts',(5.23190336064351,-1.3486493481772,339.729728110384));
#24614=CARTESIAN_POINT('',(5.23167681249902,-4.9112521298426,335.262270050933));
#24615=CARTESIAN_POINT('Origin',(5.23167681249902,0.,335.));
#24616=CARTESIAN_POINT('',(5.24653624849023,-4.91824999747317,335.000157655271));
#24617=CARTESIAN_POINT('Ctrl Pts',(5.24642228163471,-4.91824999767384,335.000151265622));
#24618=CARTESIAN_POINT('Ctrl Pts',(5.24397986243382,-4.91824865336932,335.043859978905));
#24619=CARTESIAN_POINT('Ctrl Pts',(5.24153110386067,-4.91766464706679,335.087566327886));
#24620=CARTESIAN_POINT('Ctrl Pts',(5.23758208828115,-4.91578984846743,335.157789839972));
#24621=CARTESIAN_POINT('Ctrl Pts',(5.23608712158552,-4.91486678856396,335.184314674874));
#24622=CARTESIAN_POINT('Ctrl Pts',(5.23402713173893,-4.91330267985276,335.220768624878));
#24623=CARTESIAN_POINT('Ctrl Pts',(5.23346506070249,-4.91284612511964,335.230705351861));
#24624=CARTESIAN_POINT('Ctrl Pts',(5.23268937633593,-4.91217505978087,335.244404262925));
#24625=CARTESIAN_POINT('Ctrl Pts',(5.23247619177751,-4.91198636488289,335.248167711058));
#24626=CARTESIAN_POINT('Ctrl Pts',(5.2320676217224,-4.91161656743763,335.255377499067));
#24627=CARTESIAN_POINT('Ctrl Pts',(5.23187224807966,-4.91143616218491,335.25882387311));
#24628=CARTESIAN_POINT('Ctrl Pts',(5.23167681249902,-4.91125212984261,335.262270050933));
#24629=CARTESIAN_POINT('',(6.99653624843812,-4.91824865609062,335.003635844163));
#24630=CARTESIAN_POINT('Ctrl Pts',(6.99653624843808,-4.91824865609062,335.003635844164));
#24631=CARTESIAN_POINT('Ctrl Pts',(6.9875721074894,-4.91813125822212,335.162441305286));
#24632=CARTESIAN_POINT('Ctrl Pts',(6.97860796654071,-4.91031842803173,335.320932586525));
#24633=CARTESIAN_POINT('Ctrl Pts',(6.96964382559202,-4.89492490528823,335.478427877625));
#24634=CARTESIAN_POINT('Ctrl Pts',(6.96063104327979,-4.8794478539679,335.636777772168));
#24635=CARTESIAN_POINT('Ctrl Pts',(6.95161826096759,-4.85630772715498,335.79412071973));
#24636=CARTESIAN_POINT('Ctrl Pts',(6.94260547865537,-4.8256704477217,335.949783023898));
#24637=CARTESIAN_POINT('Ctrl Pts',(6.93353337589111,-4.79483151942994,336.106469868317));
#24638=CARTESIAN_POINT('Ctrl Pts',(6.92446127312678,-4.75639650641198,336.261453756748));
#24639=CARTESIAN_POINT('Ctrl Pts',(6.91538917036252,-4.71058301455425,336.41406885458));
#24640=CARTESIAN_POINT('Ctrl Pts',(6.91062778628924,-4.68653835411107,336.494167053976));
#24641=CARTESIAN_POINT('Ctrl Pts',(6.90586640221596,-4.66046204998375,336.57361312166));
#24642=CARTESIAN_POINT('Ctrl Pts',(6.90110501814269,-4.63239073199686,336.652313277986));
#24643=CARTESIAN_POINT('Ctrl Pts',(6.89333955794828,-4.58660851844781,336.780667328371));
#24644=CARTESIAN_POINT('Ctrl Pts',(6.8855740977539,-4.5354142221827,336.907322892402));
#24645=CARTESIAN_POINT('Ctrl Pts',(6.8778086375595,-4.4789526218565,337.031788983547));
#24646=CARTESIAN_POINT('Ctrl Pts',(6.87005276090548,-4.42256070214335,337.15610146811));
#24647=CARTESIAN_POINT('Ctrl Pts',(6.86229688425144,-4.36091457216383,337.278229502424));
#24648=CARTESIAN_POINT('Ctrl Pts',(6.85454100759742,-4.29420840917725,337.397698313185));
#24649=CARTESIAN_POINT('Ctrl Pts',(6.84679283639659,-4.22756851867525,337.517048431841));
#24650=CARTESIAN_POINT('Ctrl Pts',(6.83904466519573,-4.15587878875334,337.633744244314));
#24651=CARTESIAN_POINT('Ctrl Pts',(6.8312964939949,-4.0793808491045,337.747332333457));
#24652=CARTESIAN_POINT('Ctrl Pts',(6.82355415692612,-4.00294051002624,337.860834894301));
#24653=CARTESIAN_POINT('Ctrl Pts',(6.81581181985734,-3.92169938519247,337.971234065519));
#24654=CARTESIAN_POINT('Ctrl Pts',(6.80806948278857,-3.83594406774055,338.078102690241));
#24655=CARTESIAN_POINT('Ctrl Pts',(6.80033038945911,-3.75022467844475,338.184926541148));
#24656=CARTESIAN_POINT('Ctrl Pts',(6.7925912961297,-3.65999510250297,338.28822248214));
#24657=CARTESIAN_POINT('Ctrl Pts',(6.78485220280024,-3.56558398808006,338.387594114773));
#24658=CARTESIAN_POINT('Ctrl Pts',(6.77711469667717,-3.47119223638064,338.486945367333));
#24659=CARTESIAN_POINT('Ctrl Pts',(6.76937719055405,-3.37262092166138,338.582373628314));
#24660=CARTESIAN_POINT('Ctrl Pts',(6.76163968443097,-3.2702372611815,338.673517567411));
#24661=CARTESIAN_POINT('Ctrl Pts',(6.75390207966681,-3.16785229547017,338.764662668451));
#24662=CARTESIAN_POINT('Ctrl Pts',(6.74616447490265,-3.06165517986055,338.851523078124));
#24663=CARTESIAN_POINT('Ctrl Pts',(6.73842687013848,-2.95204776861541,338.933776434206));
#24664=CARTESIAN_POINT('Ctrl Pts',(6.73068748116974,-2.84241508313472,339.016048756986));
#24665=CARTESIAN_POINT('Ctrl Pts',(6.72294809220104,-2.72937085069569,339.093711677129));
#24666=CARTESIAN_POINT('Ctrl Pts',(6.71520870323229,-2.61334722851598,339.166485248469));
#24667=CARTESIAN_POINT('Ctrl Pts',(6.70746096922121,-2.49719850317336,339.239337288346));
#24668=CARTESIAN_POINT('Ctrl Pts',(6.69971323521017,-2.37806430335908,339.307289239703));
#24669=CARTESIAN_POINT('Ctrl Pts',(6.69196550119909,-2.25640327777048,339.370106098319));
#24670=CARTESIAN_POINT('Ctrl Pts',(6.68421357162419,-2.134676370132,339.432956973609));
#24671=CARTESIAN_POINT('Ctrl Pts',(6.67646164204922,-2.01042026567888,339.490667050703));
#24672=CARTESIAN_POINT('Ctrl Pts',(6.66870971247431,-1.88411412421237,339.543049309599));
#24673=CARTESIAN_POINT('Ctrl Pts',(6.66094518694225,-1.757602750393,339.595516683392));
#24674=CARTESIAN_POINT('Ctrl Pts',(6.65318066141019,-1.62903505135232,339.642638804876));
#24675=CARTESIAN_POINT('Ctrl Pts',(6.64541613587812,-1.49890674927308,339.684278132165));
#24676=CARTESIAN_POINT('Ctrl Pts',(6.63789975187495,-1.37293713476548,339.7245867347));
#24677=CARTESIAN_POINT('Ctrl Pts',(6.63038336787179,-1.2455054622397,339.759757597904));
#24678=CARTESIAN_POINT('Ctrl Pts',(6.62286698386862,-1.11706899699421,339.789711882614));
#24679=CARTESIAN_POINT('Ctrl Pts',(6.61508110872127,-0.984027592730366,
339.820740143115));
#24680=CARTESIAN_POINT('Ctrl Pts',(6.60729523357391,-0.849484422885444,
339.84626958899));
#24681=CARTESIAN_POINT('Ctrl Pts',(6.59950935842656,-0.713933148047497,
339.866156853475));
#24682=CARTESIAN_POINT('Ctrl Pts',(6.59173308917978,-0.578549110937317,
339.886019581849));
#24683=CARTESIAN_POINT('Ctrl Pts',(6.583956819933,-0.442159825650675,339.900253924114));
#24684=CARTESIAN_POINT('Ctrl Pts',(6.57618055068622,-0.305271916830737,
339.908766863408));
#24685=CARTESIAN_POINT('Ctrl Pts',(6.56841202985661,-0.168520405631501,
339.917271320253));
#24686=CARTESIAN_POINT('Ctrl Pts',(6.56064350902701,-0.0312716461794746,
339.920065695812));
#24687=CARTESIAN_POINT('Ctrl Pts',(6.5528749881974,0.105960125494544,339.917108450533));
#24688=CARTESIAN_POINT('Ctrl Pts',(6.54511236494098,0.243087715891905,339.914153450286));
#24689=CARTESIAN_POINT('Ctrl Pts',(6.53734974168456,0.380197956106048,339.905455529135));
#24690=CARTESIAN_POINT('Ctrl Pts',(6.52958711842814,0.516774441849578,339.891025172574));
#24691=CARTESIAN_POINT('Ctrl Pts',(6.52182790550408,0.653290925813578,339.876601155662));
#24692=CARTESIAN_POINT('Ctrl Pts',(6.51406869257998,0.789273735022939,339.856449754032));
#24693=CARTESIAN_POINT('Ctrl Pts',(6.50630947965593,0.924209640464846,339.830633457733));
#24694=CARTESIAN_POINT('Ctrl Pts',(6.49855195806881,1.0591161328615,339.804822788817));
#24695=CARTESIAN_POINT('Ctrl Pts',(6.49079443648172,1.19297579291594,339.773349754805));
#24696=CARTESIAN_POINT('Ctrl Pts',(6.4830369148946,1.32528403122262,339.736328250775));
#24697=CARTESIAN_POINT('Ctrl Pts',(6.47527941721663,1.45759186174725,339.699306860846));
#24698=CARTESIAN_POINT('Ctrl Pts',(6.46752191953871,1.58834790469237,339.656737139788));
#24699=CARTESIAN_POINT('Ctrl Pts',(6.45976442186074,1.7170615883802,339.608783197788));
#24700=CARTESIAN_POINT('Ctrl Pts',(6.45200528104205,1.84580253533055,339.560819098507));
#24701=CARTESIAN_POINT('Ctrl Pts',(6.44424614022329,1.97249989704015,339.507468644903));
#24702=CARTESIAN_POINT('Ctrl Pts',(6.43648699940459,2.09668233708145,339.448944396132));
#24703=CARTESIAN_POINT('Ctrl Pts',(6.4287198465573,2.2209930069466,339.390359715675));
#24704=CARTESIAN_POINT('Ctrl Pts',(6.42095269371003,2.34278321442726,339.326590734277));
#24705=CARTESIAN_POINT('Ctrl Pts',(6.41318554086274,2.46160504845533,339.257896622503));
#24706=CARTESIAN_POINT('Ctrl Pts',(6.40541434316659,2.5804887605448,339.18916673735));
#24707=CARTESIAN_POINT('Ctrl Pts',(6.39764314547041,2.69640068985791,339.115506819574));
#24708=CARTESIAN_POINT('Ctrl Pts',(6.38987194777425,2.80892209012275,339.037219309639));
#24709=CARTESIAN_POINT('Ctrl Pts',(6.38208860479573,2.92161934541431,338.958809447403));
#24710=CARTESIAN_POINT('Ctrl Pts',(6.37430526181726,3.03091517216052,338.875757776469));
#24711=CARTESIAN_POINT('Ctrl Pts',(6.36652191883874,3.1364234047622,338.788407487132));
#24712=CARTESIAN_POINT('Ctrl Pts',(6.35922426242407,3.23534784283099,338.70650792276));
#24713=CARTESIAN_POINT('Ctrl Pts',(6.35192660600942,3.33094277749661,338.620830027704));
#24714=CARTESIAN_POINT('Ctrl Pts',(6.34462894959475,3.42292067035136,338.531684746262));
#24715=CARTESIAN_POINT('Ctrl Pts',(6.33684095463579,3.52107867138376,338.436549683301));
#24716=CARTESIAN_POINT('Ctrl Pts',(6.32905295967686,3.61541782527226,338.337173565241));
#24717=CARTESIAN_POINT('Ctrl Pts',(6.32126496471793,3.70555070628905,338.233895023902));
#24718=CARTESIAN_POINT('Ctrl Pts',(6.31348639933423,3.79557445590721,338.13074153051));
#24719=CARTESIAN_POINT('Ctrl Pts',(6.3057078339505,3.88140181321909,338.023695306643));
#24720=CARTESIAN_POINT('Ctrl Pts',(6.2979292685668,3.962680769067,337.913133053083));
#24721=CARTESIAN_POINT('Ctrl Pts',(6.2901582801599,4.04388055237707,337.802678496456));
#24722=CARTESIAN_POINT('Ctrl Pts',(6.28238729175301,4.12054052275392,337.688715038205));
#24723=CARTESIAN_POINT('Ctrl Pts',(6.27461630334611,4.19234791897143,337.571653551471));
#24724=CARTESIAN_POINT('Ctrl Pts',(6.26685104578577,4.26410235961257,337.454678393707));
#24725=CARTESIAN_POINT('Ctrl Pts',(6.25908578822542,4.33101114693228,337.33461008598));
#24726=CARTESIAN_POINT('Ctrl Pts',(6.25132053066508,4.39280416044029,337.211889389305));
#24727=CARTESIAN_POINT('Ctrl Pts',(6.24355844243135,4.4545719536333,337.089218780082));
#24728=CARTESIAN_POINT('Ctrl Pts',(6.23579635419759,4.51122795118491,336.963898282126));
#24729=CARTESIAN_POINT('Ctrl Pts',(6.22803426596386,4.5625475281804,336.836394052374));
#24730=CARTESIAN_POINT('Ctrl Pts',(6.22027372317695,4.61385688734857,336.708915208962));
#24731=CARTESIAN_POINT('Ctrl Pts',(6.21251318039004,4.6598317942243,336.579253859601));
#24732=CARTESIAN_POINT('Ctrl Pts',(6.20475263760312,4.70029556895248,336.44789662165));
#24733=CARTESIAN_POINT('Ctrl Pts',(6.19699197664848,4.7407599598118,336.316537383558));
#24734=CARTESIAN_POINT('Ctrl Pts',(6.18923131569386,4.77571293670882,336.183482577497));
#24735=CARTESIAN_POINT('Ctrl Pts',(6.18147065473923,4.80502766201519,336.049234115805));
#24736=CARTESIAN_POINT('Ctrl Pts',(6.17370821228768,4.83434911665723,335.914954836735));
#24737=CARTESIAN_POINT('Ctrl Pts',(6.16594576983614,4.85802966096728,335.779481737024));
#24738=CARTESIAN_POINT('Ctrl Pts',(6.15818332738459,4.87599362602538,335.643326683311));
#24739=CARTESIAN_POINT('Ctrl Pts',(6.15041267564842,4.89397658913765,335.507027636828));
#24740=CARTESIAN_POINT('Ctrl Pts',(6.14264202391224,4.90623084514752,335.370045582226));
#24741=CARTESIAN_POINT('Ctrl Pts',(6.13487137217606,4.91273260609387,335.232897839239));
#24742=CARTESIAN_POINT('Ctrl Pts',(6.12709656270277,4.91923784584918,335.095676714471));
#24743=CARTESIAN_POINT('Ctrl Pts',(6.11932175322947,4.91998445487191,334.958290113788));
#24744=CARTESIAN_POINT('Ctrl Pts',(6.11154694375617,4.91500081266808,334.821254163763));
#24745=CARTESIAN_POINT('Ctrl Pts',(6.10375983529211,4.91000928682805,334.684001436222));
#24746=CARTESIAN_POINT('Ctrl Pts',(6.09597272682799,4.89926942609259,334.547100856136));
#24747=CARTESIAN_POINT('Ctrl Pts',(6.08818561836392,4.88286150040578,334.41106313551));
#24748=CARTESIAN_POINT('Ctrl Pts',(6.08092071734951,4.86755389855118,334.28414817354));
#24749=CARTESIAN_POINT('Ctrl Pts',(6.07365581633523,4.84731351523526,334.157984389752));
#24750=CARTESIAN_POINT('Ctrl Pts',(6.06639091532082,4.82224507075424,334.032975936139));
#24751=CARTESIAN_POINT('Ctrl Pts',(6.05868386149048,4.79565092299157,333.900359279789));
#24752=CARTESIAN_POINT('Ctrl Pts',(6.05097680766012,4.76353558103867,333.768609417271));
#24753=CARTESIAN_POINT('Ctrl Pts',(6.04326975382978,4.72596638014111,333.638227318428));
#24754=CARTESIAN_POINT('Ctrl Pts',(6.03557234821298,4.68844421092145,333.508008440753));
#24755=CARTESIAN_POINT('Ctrl Pts',(6.02787494259624,4.64548187143294,333.379154299647));
#24756=CARTESIAN_POINT('Ctrl Pts',(6.02017753697945,4.59719799306904,333.2521574227));
#24757=CARTESIAN_POINT('Ctrl Pts',(6.01248784812709,4.54896252001646,333.125287862025));
#24758=CARTESIAN_POINT('Ctrl Pts',(6.00479815927465,4.4954162614158,333.000272231084));
#24759=CARTESIAN_POINT('Ctrl Pts',(5.99710847042229,4.43672799044302,332.877589153505));
#24760=CARTESIAN_POINT('Ctrl Pts',(5.98942457450589,4.37808393158358,332.754998497768));
#24761=CARTESIAN_POINT('Ctrl Pts',(5.98174067858953,4.31430573899637,332.6347372567));
#24762=CARTESIAN_POINT('Ctrl Pts',(5.97405678267313,4.24561058229956,332.517264845787));
#24763=CARTESIAN_POINT('Ctrl Pts',(5.96631078677204,4.17636024262972,332.398843042144));
#24764=CARTESIAN_POINT('Ctrl Pts',(5.95856479087094,4.10211325683485,332.283255729738));
#24765=CARTESIAN_POINT('Ctrl Pts',(5.95081879496985,4.02313991562323,332.170949226009));
#24766=CARTESIAN_POINT('Ctrl Pts',(5.94313933023576,3.94484488467923,332.059607334558));
#24767=CARTESIAN_POINT('Ctrl Pts',(5.9354598655017,3.86190462297316,331.951490431564));
#24768=CARTESIAN_POINT('Ctrl Pts',(5.9277804007676,3.77462613599108,331.847004504286));
#24769=CARTESIAN_POINT('Ctrl Pts',(5.92010062424812,3.68734410551248,331.742514334892));
#24770=CARTESIAN_POINT('Ctrl Pts',(5.91242084772856,3.59572375435876,331.641655740437));
#24771=CARTESIAN_POINT('Ctrl Pts',(5.90474107120909,3.50011199266095,331.5448011488));
#24772=CARTESIAN_POINT('Ctrl Pts',(5.89705925050953,3.40447478130869,331.447920776696));
#24773=CARTESIAN_POINT('Ctrl Pts',(5.88937742981002,3.30484432563591,331.355046810899));
#24774=CARTESIAN_POINT('Ctrl Pts',(5.88169560911047,3.20160358580878,331.266514022815));
#24775=CARTESIAN_POINT('Ctrl Pts',(5.87390038177184,3.09683870401358,331.176674226102));
#24776=CARTESIAN_POINT('Ctrl Pts',(5.86610515443318,2.98835641543208,331.09130508047));
#24777=CARTESIAN_POINT('Ctrl Pts',(5.85830992709455,2.87658965774756,331.010712469195));
#24778=CARTESIAN_POINT('Ctrl Pts',(5.85061448468494,2.76625360086214,330.931151505573));
#24779=CARTESIAN_POINT('Ctrl Pts',(5.84291904227532,2.65271704010501,330.856245667595));
#24780=CARTESIAN_POINT('Ctrl Pts',(5.83522359986571,2.53642289726112,330.786243724567));
#24781=CARTESIAN_POINT('Ctrl Pts',(5.82737848006257,2.41786681764243,330.714880234299));
#24782=CARTESIAN_POINT('Ctrl Pts',(5.81953336025945,2.29644516878371,330.648613573096));
#24783=CARTESIAN_POINT('Ctrl Pts',(5.81168824045631,2.17264941458252,330.587656225563));
#24784=CARTESIAN_POINT('Ctrl Pts',(5.80384312065317,2.04885366038149,330.52669887803));
#24785=CARTESIAN_POINT('Ctrl Pts',(5.79599800085003,1.92268422390205,330.471050949101));
#24786=CARTESIAN_POINT('Ctrl Pts',(5.7881528810469,1.79464876300254,330.420871384209));
#24787=CARTESIAN_POINT('Ctrl Pts',(5.78026078471884,1.66584662661929,330.370391344419));
#24788=CARTESIAN_POINT('Ctrl Pts',(5.77236868839078,1.53472896145545,330.325277599703));
#24789=CARTESIAN_POINT('Ctrl Pts',(5.76447659206272,1.40177576443656,330.285744197783));
#24790=CARTESIAN_POINT('Ctrl Pts',(5.75659477697891,1.26899576909125,330.246262297079));
#24791=CARTESIAN_POINT('Ctrl Pts',(5.74871296189506,1.13438536093766,330.212346373245));
#24792=CARTESIAN_POINT('Ctrl Pts',(5.74083114681125,0.998444213537087,330.184162355835));
#24793=CARTESIAN_POINT('Ctrl Pts',(5.73295789406051,0.862650744478501,330.156008955859));
#24794=CARTESIAN_POINT('Ctrl Pts',(5.72508464130977,0.72552978188081,330.133575140134));
#24795=CARTESIAN_POINT('Ctrl Pts',(5.71721138855904,0.587595675319844,330.116976921533));
#24796=CARTESIAN_POINT('Ctrl Pts',(5.70934498637394,0.4497815860733,330.100393145143));
#24797=CARTESIAN_POINT('Ctrl Pts',(5.70147858418885,0.311156135015818,330.089634898965));
#24798=CARTESIAN_POINT('Ctrl Pts',(5.69361218200376,0.172243187547443,330.084767009913));
#24799=CARTESIAN_POINT('Ctrl Pts',(5.68575106428807,0.0334235586259079,
330.079902390997));
#24800=CARTESIAN_POINT('Ctrl Pts',(5.6778899465724,-0.105682805793181,330.080920259691));
#24801=CARTESIAN_POINT('Ctrl Pts',(5.67002882885672,-0.244547816333455,
330.087833530098));
#24802=CARTESIAN_POINT('Ctrl Pts',(5.66217060126191,-0.383361773488972,
330.094744258859));
#24803=CARTESIAN_POINT('Ctrl Pts',(5.6543123736671,-0.521934177033776,330.107546055514));
#24804=CARTESIAN_POINT('Ctrl Pts',(5.6464541460723,-0.659737884083653,330.126199738725));
#24805=CARTESIAN_POINT('Ctrl Pts',(5.6385972681182,-0.797517923520168,330.144850218189));
#24806=CARTESIAN_POINT('Ctrl Pts',(5.63074039016412,-0.934529155614134,
330.169350531977));
#24807=CARTESIAN_POINT('Ctrl Pts',(5.62288351221002,-1.0702507171905,330.199609759108));
#24808=CARTESIAN_POINT('Ctrl Pts',(5.61502644467577,-1.2059755536192,330.229869716369));
#24809=CARTESIAN_POINT('Ctrl Pts',(5.60716937714152,-1.34041028952876,330.265888780584));
#24810=CARTESIAN_POINT('Ctrl Pts',(5.59931230960726,-1.47304560802506,330.30752520527));
#24811=CARTESIAN_POINT('Ctrl Pts',(5.5914500955778,-1.60576780461264,330.349188902428));
#24812=CARTESIAN_POINT('Ctrl Pts',(5.58358788154838,-1.73668786801434,330.396477199504));
#24813=CARTESIAN_POINT('Ctrl Pts',(5.57572566751892,-1.86531252992189,330.449198726794));
#24814=CARTESIAN_POINT('Ctrl Pts',(5.56786087237617,-1.99397941846229,330.501937562214));
#24815=CARTESIAN_POINT('Ctrl Pts',(5.55999607723336,-2.12034905829143,330.560113030222));
#24816=CARTESIAN_POINT('Ctrl Pts',(5.55213128209061,-2.24394998899759,330.623486375049));
#24817=CARTESIAN_POINT('Ctrl Pts',(5.54425770267667,-2.36768897086402,330.686930502223));
#24818=CARTESIAN_POINT('Ctrl Pts',(5.53638412326274,-2.48865273318168,330.755583925014));
#24819=CARTESIAN_POINT('Ctrl Pts',(5.5285105438488,-2.60639555360929,330.829162520473));
#24820=CARTESIAN_POINT('Ctrl Pts',(5.52231197815687,-2.69908993932676,330.887088113586));
#24821=CARTESIAN_POINT('Ctrl Pts',(5.51611341246493,-2.78978853945073,330.948065313056));
#24822=CARTESIAN_POINT('Ctrl Pts',(5.509914846773,-2.87828766110725,331.011937412425));
#24823=CARTESIAN_POINT('Ctrl Pts',(5.50212555639797,-2.98949812345911,331.092200872324));
#24824=CARTESIAN_POINT('Ctrl Pts',(5.49433626602291,-3.09747411330485,331.177210125069));
#24825=CARTESIAN_POINT('Ctrl Pts',(5.48654697564788,-3.20178911311133,331.266673127402));
#24826=CARTESIAN_POINT('Ctrl Pts',(5.47876407696554,-3.30601851469403,331.356062718681));
#24827=CARTESIAN_POINT('Ctrl Pts',(5.47098117828319,-3.40659261136152,331.449898535112));
#24828=CARTESIAN_POINT('Ctrl Pts',(5.46319827960085,-3.50311582346135,331.547846673464));
#24829=CARTESIAN_POINT('Ctrl Pts',(5.45541994514562,-3.5995824301908,331.645737370807));
#24830=CARTESIAN_POINT('Ctrl Pts',(5.44764161069039,-3.69200260886747,331.747735314344));
#24831=CARTESIAN_POINT('Ctrl Pts',(5.43986327623517,-3.78001594856677,331.853468180507));
#24832=CARTESIAN_POINT('Ctrl Pts',(5.4320878010631,-3.8679969349313,331.959162179712));
#24833=CARTESIAN_POINT('Ctrl Pts',(5.42431232589101,-3.95157405965888,332.068588069951));
#24834=CARTESIAN_POINT('Ctrl Pts',(5.41653685071893,-4.03042593523069,332.181338998191));
#24835=CARTESIAN_POINT('Ctrl Pts',(5.4087605973133,-4.10928570294714,332.294101211471));
#24836=CARTESIAN_POINT('Ctrl Pts',(5.40098434390764,-4.18341904663606,332.410188814677));
#24837=CARTESIAN_POINT('Ctrl Pts',(5.39320809050201,-4.25254681278462,332.529164378682));
#24838=CARTESIAN_POINT('Ctrl Pts',(5.38573733687997,-4.31895880869057,332.643465839727));
#24839=CARTESIAN_POINT('Ctrl Pts',(5.37826658325798,-4.38075090673827,332.760432357873));
#24840=CARTESIAN_POINT('Ctrl Pts',(5.37079582963594,-4.43771507093567,332.879653799095));
#24841=CARTESIAN_POINT('Ctrl Pts',(5.36187472659634,-4.50573808495532,333.02202052881));
#24842=CARTESIAN_POINT('Ctrl Pts',(5.35295362355671,-4.56683857097974,333.167520696865));
#24843=CARTESIAN_POINT('Ctrl Pts',(5.34403252051712,-4.62078803516182,333.315511651389));
#24844=CARTESIAN_POINT('Ctrl Pts',(5.33507957933183,-4.67493003729503,333.464030764545));
#24845=CARTESIAN_POINT('Ctrl Pts',(5.32612663814647,-4.72186985838296,333.615058315507));
#24846=CARTESIAN_POINT('Ctrl Pts',(5.31717369696119,-4.76142762282966,333.76793260937));
#24847=CARTESIAN_POINT('Ctrl Pts',(5.30821146906304,-4.80102641978095,333.920965476783));
#24848=CARTESIAN_POINT('Ctrl Pts',(5.29924924116492,-4.83322782295187,334.075848763131));
#24849=CARTESIAN_POINT('Ctrl Pts',(5.29028701326675,-4.85790275767711,334.231908951066));
#24850=CARTESIAN_POINT('Ctrl Pts',(5.28132449551006,-4.88257849044498,334.387974186336));
#24851=CARTESIAN_POINT('Ctrl Pts',(5.27236197775338,-4.89972725055652,334.545216245031));
#24852=CARTESIAN_POINT('Ctrl Pts',(5.26339945999669,-4.9092715151488,334.70295412299));
#24853=CARTESIAN_POINT('Ctrl Pts',(5.25777838949452,-4.9152574429451,334.801883436933));
#24854=CARTESIAN_POINT('Ctrl Pts',(5.2521573189924,-4.91825317574233,334.901007641494));
#24855=CARTESIAN_POINT('Ctrl Pts',(5.24653624849023,-4.91824999747317,335.000157655271));
#24856=CARTESIAN_POINT('',(8.74653624854529,-4.91824892942493,334.996754894379));
#24857=CARTESIAN_POINT('Ctrl Pts',(8.74653624849026,-4.91824892942558,334.996754895354));
#24858=CARTESIAN_POINT('Ctrl Pts',(8.73874364056494,-4.91834007680728,335.134896977485));
#24859=CARTESIAN_POINT('Ctrl Pts',(8.73095103263955,-4.91260676554203,335.27307124222));
#24860=CARTESIAN_POINT('Ctrl Pts',(8.72315842471423,-4.90106754548729,335.410755373758));
#24861=CARTESIAN_POINT('Ctrl Pts',(8.71536551879347,-4.88952788416372,335.548444770446));
#24862=CARTESIAN_POINT('Ctrl Pts',(8.70757261287277,-4.87218190333353,335.685643613584));
#24863=CARTESIAN_POINT('Ctrl Pts',(8.699779706952,-4.84910010958536,335.821834040253));
#24864=CARTESIAN_POINT('Ctrl Pts',(8.69198489074262,-4.82601265775683,335.95805785152));
#24865=CARTESIAN_POINT('Ctrl Pts',(8.68419007453323,-4.79718665772279,336.093272375284));
#24866=CARTESIAN_POINT('Ctrl Pts',(8.67639525832385,-4.76274382037261,336.226969585606));
#24867=CARTESIAN_POINT('Ctrl Pts',(8.66859691864463,-4.7282854139191,336.360727230719));
#24868=CARTESIAN_POINT('Ctrl Pts',(8.66079857896543,-4.68820521096132,336.492965825072));
#24869=CARTESIAN_POINT('Ctrl Pts',(8.6530002392862,-4.64267480297804,336.623192452019));
#24870=CARTESIAN_POINT('Ctrl Pts',(8.64519192752529,-4.59708617324934,336.753585605512));
#24871=CARTESIAN_POINT('Ctrl Pts',(8.63738361576436,-4.54603354725092,336.881961290696));
#24872=CARTESIAN_POINT('Ctrl Pts',(8.62957530400345,-4.48973694012501,337.007845928097));
#24873=CARTESIAN_POINT('Ctrl Pts',(8.62176139640016,-4.43339998792199,337.133820780978));
#24874=CARTESIAN_POINT('Ctrl Pts',(8.61394748879692,-4.37181173745019,337.257300685956));
#24875=CARTESIAN_POINT('Ctrl Pts',(8.60613358119363,-4.3052377803483,337.377837403432));
#24876=CARTESIAN_POINT('Ctrl Pts',(8.59830717128388,-4.23855730445237,337.498566980494));
#24877=CARTESIAN_POINT('Ctrl Pts',(8.59048076137409,-4.16687538867154,337.616343637309));
#24878=CARTESIAN_POINT('Ctrl Pts',(8.58265435146433,-4.09050086762669,337.730748196822));
#24879=CARTESIAN_POINT('Ctrl Pts',(8.57861397557166,-4.05107260138437,337.789809430465));
#24880=CARTESIAN_POINT('Ctrl Pts',(8.57457359967899,-4.01039435681843,337.847972493624));
#24881=CARTESIAN_POINT('Ctrl Pts',(8.57053322378633,-3.9685126605159,337.905183354941));
#24882=CARTESIAN_POINT('Ctrl Pts',(8.56275835230203,-3.88791995950315,338.01527387772));
#24883=CARTESIAN_POINT('Ctrl Pts',(8.55498348081771,-3.80261536607146,338.122182290313));
#24884=CARTESIAN_POINT('Ctrl Pts',(8.54720860933341,-3.71287886078536,338.225478821452));
#24885=CARTESIAN_POINT('Ctrl Pts',(8.53944330571045,-3.62325278644864,338.328648234491));
#24886=CARTESIAN_POINT('Ctrl Pts',(8.53167800208752,-3.52920590598831,338.42821431773));
#24887=CARTESIAN_POINT('Ctrl Pts',(8.52391269846456,-3.43106087603816,338.523776997402));
#24888=CARTESIAN_POINT('Ctrl Pts',(8.51615509428656,-3.33301315873585,338.619244924876));
#24889=CARTESIAN_POINT('Ctrl Pts',(8.50839749010855,-3.23087565657685,338.710717077265));
#24890=CARTESIAN_POINT('Ctrl Pts',(8.50063988593055,-3.12501037171476,338.797827436729));
#24891=CARTESIAN_POINT('Ctrl Pts',(8.49288811945772,-3.01922475195361,338.884872244436));
#24892=CARTESIAN_POINT('Ctrl Pts',(8.48513635298485,-2.90971723374499,338.967561545116));
#24893=CARTESIAN_POINT('Ctrl Pts',(8.47738458651202,-2.79688538493468,339.0455673528));
#24894=CARTESIAN_POINT('Ctrl Pts',(8.46963610183688,-2.68410130475901,339.123540135845));
#24895=CARTESIAN_POINT('Ctrl Pts',(8.46188761716177,-2.56799601404754,339.196833147722));
#24896=CARTESIAN_POINT('Ctrl Pts',(8.45413913248663,-2.44899857882953,339.265159905958));
#24897=CARTESIAN_POINT('Ctrl Pts',(8.44639225925284,-2.33002589133903,339.333472454375));
#24898=CARTESIAN_POINT('Ctrl Pts',(8.43864538601905,-2.20816259449402,339.396820608989));
#24899=CARTESIAN_POINT('Ctrl Pts',(8.43089851278526,-2.08386469503069,339.454962513344));
#24900=CARTESIAN_POINT('Ctrl Pts',(8.42315157369512,-1.959565738908,339.513104911966));
#24901=CARTESIAN_POINT('Ctrl Pts',(8.41540463460496,-1.83283249296259,339.566040806431));
#24902=CARTESIAN_POINT('Ctrl Pts',(8.40765769551481,-1.70414303495464,339.613575574207));
#24903=CARTESIAN_POINT('Ctrl Pts',(8.39990901358327,-1.57542462547148,339.661121035956));
#24904=CARTESIAN_POINT('Ctrl Pts',(8.39216033165171,-1.44474949480223,339.703262817687));
#24905=CARTESIAN_POINT('Ctrl Pts',(8.38441164972016,-1.31261266715699,339.739855593636));
#24906=CARTESIAN_POINT('Ctrl Pts',(8.37665474013633,-1.18033553489204,339.776487224274));
#24907=CARTESIAN_POINT('Ctrl Pts',(8.36889783055252,-1.04659398260185,339.807557974806));
#24908=CARTESIAN_POINT('Ctrl Pts',(8.36114092096869,-0.911895608651636,
339.832973149255));
#24909=CARTESIAN_POINT('Ctrl Pts',(8.35337986496807,-0.777125232366675,
339.858401909258));
#24910=CARTESIAN_POINT('Ctrl Pts',(8.34561880896741,-0.641397401904383,
339.878169012965));
#24911=CARTESIAN_POINT('Ctrl Pts',(8.33785775296678,-0.505225718564822,
339.892231600793));
#24912=CARTESIAN_POINT('Ctrl Pts',(8.33008427732382,-0.368836126270194,
339.906316692301));
#24913=CARTESIAN_POINT('Ctrl Pts',(8.3223108016809,-0.232001652130057,339.91467900231));
#24914=CARTESIAN_POINT('Ctrl Pts',(8.31453732603794,-0.0952376816340296,
339.917327815643));
#24915=CARTESIAN_POINT('Ctrl Pts',(8.30712328052938,0.0352025934450748,
339.919854153088));
#24916=CARTESIAN_POINT('Ctrl Pts',(8.29970923502085,0.165578450703937,339.917183551418));
#24917=CARTESIAN_POINT('Ctrl Pts',(8.29229518951229,0.295448212965507,339.909367924281));
#24918=CARTESIAN_POINT('Ctrl Pts',(8.28451997644765,0.431644446327098,339.901171566953));
#24919=CARTESIAN_POINT('Ctrl Pts',(8.27674476338299,0.56771454764716,339.887290407692));
#24920=CARTESIAN_POINT('Ctrl Pts',(8.26896955031836,0.703145564399604,339.867727331904));
#24921=CARTESIAN_POINT('Ctrl Pts',(8.26120390615335,0.838409907159359,339.848188332254));
#24922=CARTESIAN_POINT('Ctrl Pts',(8.25343826198836,0.973036347147702,339.822981384888));
#24923=CARTESIAN_POINT('Ctrl Pts',(8.24567261782335,1.10651381254502,339.79216133338));
#24924=CARTESIAN_POINT('Ctrl Pts',(8.23791467447588,1.23985891473,339.761371844643));
#24925=CARTESIAN_POINT('Ctrl Pts',(8.23015673112841,1.37205693137504,339.724980416286));
#24926=CARTESIAN_POINT('Ctrl Pts',(8.22239878778095,1.50260413832473,339.68309340778));
#24927=CARTESIAN_POINT('Ctrl Pts',(8.21464668384396,1.63305308228202,339.641237927659));
#24928=CARTESIAN_POINT('Ctrl Pts',(8.20689457990702,1.76185331913804,339.593895219883));
#24929=CARTESIAN_POINT('Ctrl Pts',(8.19914247597004,1.88851386084796,339.54122213285));
#24930=CARTESIAN_POINT('Ctrl Pts',(8.19139365757884,2.01512072048488,339.488571370058));
#24931=CARTESIAN_POINT('Ctrl Pts',(8.18364483918755,2.13958932851358,339.430594871093));
#24932=CARTESIAN_POINT('Ctrl Pts',(8.17589602079636,2.26144655336154,339.367498431458));
#24933=CARTESIAN_POINT('Ctrl Pts',(8.16814881617046,2.38327840028077,339.304415132259));
#24934=CARTESIAN_POINT('Ctrl Pts',(8.16040161154464,2.50249959889433,339.236214192899));
#24935=CARTESIAN_POINT('Ctrl Pts',(8.15265440691874,2.61865996541526,339.163148213556));
#24936=CARTESIAN_POINT('Ctrl Pts',(8.14490713906141,2.73482128001834,339.090081637859));
#24937=CARTESIAN_POINT('Ctrl Pts',(8.13715987120404,2.84792138184613,339.012150151083));
#24938=CARTESIAN_POINT('Ctrl Pts',(8.12941260334671,2.95753786279379,338.929650474615));
#24939=CARTESIAN_POINT('Ctrl Pts',(8.12166359557585,3.06717896186511,338.847132270027));
#24940=CARTESIAN_POINT('Ctrl Pts',(8.113914587805,3.17333457100083,338.76004406923));
#24941=CARTESIAN_POINT('Ctrl Pts',(8.10616558003414,3.27561456532418,338.668723522144));
#24942=CARTESIAN_POINT('Ctrl Pts',(8.09840835104594,3.37800307238731,338.577306089614));
#24943=CARTESIAN_POINT('Ctrl Pts',(8.09065112205773,3.47650745893542,338.481647601813));
#24944=CARTESIAN_POINT('Ctrl Pts',(8.08289389306952,3.5707733705158,338.382123681789));
#24945=CARTESIAN_POINT('Ctrl Pts',(8.07513252066287,3.66508963295176,338.282546602415));
#24946=CARTESIAN_POINT('Ctrl Pts',(8.06737114825622,3.75516265280226,338.179100271403));
#24947=CARTESIAN_POINT('Ctrl Pts',(8.05960977584957,3.84067841605557,338.07219341301));
#24948=CARTESIAN_POINT('Ctrl Pts',(8.05183599209126,3.9263309291198,337.965115597918));
#24949=CARTESIAN_POINT('Ctrl Pts',(8.04406220833293,4.00741139153291,337.85456651263));
#24950=CARTESIAN_POINT('Ctrl Pts',(8.03628842457462,4.08364867213382,337.740984601394));
#24951=CARTESIAN_POINT('Ctrl Pts',(8.02887800146253,4.156322485007,337.632711713145));
#24952=CARTESIAN_POINT('Ctrl Pts',(8.02146757835047,4.22459548850642,337.521683354024));
#24953=CARTESIAN_POINT('Ctrl Pts',(8.01405715523839,4.28827258877716,337.408298417315));
#24954=CARTESIAN_POINT('Ctrl Pts',(8.00628161170165,4.35508713606542,337.289326868936));
#24955=CARTESIAN_POINT('Ctrl Pts',(7.99850606816487,4.41705239200587,337.167384885051));
#24956=CARTESIAN_POINT('Ctrl Pts',(7.99073052462813,4.4738932078585,337.042905437649));
#24957=CARTESIAN_POINT('Ctrl Pts',(7.98296454595626,4.53066410258984,336.918579115118));
#24958=CARTESIAN_POINT('Ctrl Pts',(7.97519856728445,4.58232293900728,336.791721891872));
#24959=CARTESIAN_POINT('Ctrl Pts',(7.96743258861258,4.62863928146743,336.662793271744));
#24960=CARTESIAN_POINT('Ctrl Pts',(7.95967430711986,4.67490971790587,336.533992438045));
#24961=CARTESIAN_POINT('Ctrl Pts',(7.95191602562709,4.71584806681081,336.403124658593));
#24962=CARTESIAN_POINT('Ctrl Pts',(7.94415774413437,4.75127119149535,336.270671132656));
#24963=CARTESIAN_POINT('Ctrl Pts',(7.93640529880406,4.78666766915647,336.138317244802));
#24964=CARTESIAN_POINT('Ctrl Pts',(7.92865285347378,4.81655708008462,336.004380360865));
#24965=CARTESIAN_POINT('Ctrl Pts',(7.92090040814347,4.84080563832996,335.869358288862));
#24966=CARTESIAN_POINT('Ctrl Pts',(7.91315124466932,4.86504393139098,335.734393375987));
#24967=CARTESIAN_POINT('Ctrl Pts',(7.90540208119514,4.88364605231357,335.598344572619));
#24968=CARTESIAN_POINT('Ctrl Pts',(7.89765291772099,4.89652903970712,335.461721155899));
#24969=CARTESIAN_POINT('Ctrl Pts',(7.8899053658207,4.90940934785847,335.325126152405));
#24970=CARTESIAN_POINT('Ctrl Pts',(7.88215781392046,4.91657285161,335.187957162106));
#24971=CARTESIAN_POINT('Ctrl Pts',(7.87441026202018,4.91798836733782,335.050729490732));
#24972=CARTESIAN_POINT('Ctrl Pts',(7.86666264503729,4.91940389495654,334.913500666589));
#24973=CARTESIAN_POINT('Ctrl Pts',(7.85891502805435,4.91507133421292,334.776213551186));
#24974=CARTESIAN_POINT('Ctrl Pts',(7.85116741107146,4.90501163499754,334.639383967302));
#24975=CARTESIAN_POINT('Ctrl Pts',(7.84341805266317,4.89494967467197,334.502523628347));
#24976=CARTESIAN_POINT('Ctrl Pts',(7.83566869425488,4.87915804296702,334.366121415241));
#24977=CARTESIAN_POINT('Ctrl Pts',(7.82791933584659,4.85770957758364,334.230688150129));
#24978=CARTESIAN_POINT('Ctrl Pts',(7.8201617558454,4.83623835669697,334.095111198648));
#24979=CARTESIAN_POINT('Ctrl Pts',(7.81240417584421,4.80909837469085,333.960505635297));
#24980=CARTESIAN_POINT('Ctrl Pts',(7.80464659584302,4.77641375883196,333.827372750214));
#24981=CARTESIAN_POINT('Ctrl Pts',(7.79688487166486,4.74371168252373,333.69416874421));
#24982=CARTESIAN_POINT('Ctrl Pts',(7.78912314748676,4.70545917922386,333.562439359217));
#24983=CARTESIAN_POINT('Ctrl Pts',(7.7813614233086,4.66183004198195,333.43266987454));
#24984=CARTESIAN_POINT('Ctrl Pts',(7.77358729007109,4.61813115264107,333.302692920852));
#24985=CARTESIAN_POINT('Ctrl Pts',(7.76581315683357,4.56903859222243,333.174682494026));
#24986=CARTESIAN_POINT('Ctrl Pts',(7.75803902359607,4.51477435199853,333.049103894864));
#24987=CARTESIAN_POINT('Ctrl Pts',(7.75063238938553,4.46307529233841,332.929461650481));
#24988=CARTESIAN_POINT('Ctrl Pts',(7.74322575517492,4.40668244441044,332.812026836026));
#24989=CARTESIAN_POINT('Ctrl Pts',(7.73581912096438,4.34582529282009,332.697178776634));
#24990=CARTESIAN_POINT('Ctrl Pts',(7.72804547000375,4.28195252126459,332.576639716401));
#24991=CARTESIAN_POINT('Ctrl Pts',(7.72027181904308,4.21295976613436,332.458569235784));
#24992=CARTESIAN_POINT('Ctrl Pts',(7.71249816808239,4.13906200126668,332.343432889579));
#24993=CARTESIAN_POINT('Ctrl Pts',(7.70473408651929,4.06525520486368,332.228438276709));
#24994=CARTESIAN_POINT('Ctrl Pts',(7.69697000495611,3.98655562188279,332.116370937523));
#24995=CARTESIAN_POINT('Ctrl Pts',(7.68920592339302,3.90322474152287,332.007673199722));
#24996=CARTESIAN_POINT('Ctrl Pts',(7.68144954154498,3.819976501206,331.899083258522));
#24997=CARTESIAN_POINT('Ctrl Pts',(7.67369315969695,3.73210633994887,331.793856576977));
#24998=CARTESIAN_POINT('Ctrl Pts',(7.66593677784891,3.63991959477862,331.692407460698));
#24999=CARTESIAN_POINT('Ctrl Pts',(7.65818623272046,3.54780222063615,331.591034685431));
#25000=CARTESIAN_POINT('Ctrl Pts',(7.65043568759202,3.45137498993476,331.493434105567));
#25001=CARTESIAN_POINT('Ctrl Pts',(7.64268514246356,3.35098391989302,331.399987523477));
#25002=CARTESIAN_POINT('Ctrl Pts',(7.63493787337777,3.25063528369594,331.306580439899));
#25003=CARTESIAN_POINT('Ctrl Pts',(7.62719060429197,3.1463264260956,331.217324127791));
#25004=CARTESIAN_POINT('Ctrl Pts',(7.61944333520617,3.0384405196533,331.132563863355));
#25005=CARTESIAN_POINT('Ctrl Pts',(7.61169767389807,2.93057700259133,331.047821189073));
#25006=CARTESIAN_POINT('Ctrl Pts',(7.60395201259002,2.81913822052735,330.967572947991));
#25007=CARTESIAN_POINT('Ctrl Pts',(7.59620635128192,2.70454044007389,330.892124141298));
#25008=CARTESIAN_POINT('Ctrl Pts',(7.58846061933131,2.58994161445792,330.816674646493));
#25009=CARTESIAN_POINT('Ctrl Pts',(7.58071488738061,2.47218405959718,330.7460248884));
#25010=CARTESIAN_POINT('Ctrl Pts',(7.57296915543,2.35171269187729,330.680436309375));
#25011=CARTESIAN_POINT('Ctrl Pts',(7.56522167472535,2.23121412533453,330.614832922416));
#25012=CARTESIAN_POINT('Ctrl Pts',(7.55747419402075,2.10800087010399,330.554293175222));
#25013=CARTESIAN_POINT('Ctrl Pts',(7.54972671331609,1.98254171704078,330.499032170445));
#25014=CARTESIAN_POINT('Ctrl Pts',(7.54197098888234,1.85694906880536,330.443712365036));
#25015=CARTESIAN_POINT('Ctrl Pts',(7.53421526444858,1.72910610740857,330.393682680104));
#25016=CARTESIAN_POINT('Ctrl Pts',(7.52645954001483,1.59950136356103,330.349109929221));
#25017=CARTESIAN_POINT('Ctrl Pts',(7.5186996622906,1.46982721470147,330.304513309056));
#25018=CARTESIAN_POINT('Ctrl Pts',(7.5109397845664,1.33838977806884,330.265379557255));
#25019=CARTESIAN_POINT('Ctrl Pts',(7.50317990684218,1.20569099186815,330.231825056206));
#25020=CARTESIAN_POINT('Ctrl Pts',(7.49540758585675,1.07277941808026,330.198216749229));
#25021=CARTESIAN_POINT('Ctrl Pts',(7.48763526487133,0.938602835910154,330.170205650762));
#25022=CARTESIAN_POINT('Ctrl Pts',(7.47986294388591,0.803672461776946,330.147856799652));
#25023=CARTESIAN_POINT('Ctrl Pts',(7.47243565815412,0.674732027579236,330.126500077087));
#25024=CARTESIAN_POINT('Ctrl Pts',(7.4650083724223,0.545103583458626,330.110313680698));
#25025=CARTESIAN_POINT('Ctrl Pts',(7.45758108669051,0.415234142492321,330.099309878251));
#25026=CARTESIAN_POINT('Ctrl Pts',(7.4498047450077,0.279261300787976,330.087788936317));
#25027=CARTESIAN_POINT('Ctrl Pts',(7.44202840332493,0.142593965360228,330.081913076826));
#25028=CARTESIAN_POINT('Ctrl Pts',(7.43425206164218,0.00574026669514989,
330.081753349837));
#25029=CARTESIAN_POINT('Ctrl Pts',(7.42648529447328,-0.130944932733913,
330.08159381951));
#25030=CARTESIAN_POINT('Ctrl Pts',(7.41871852730447,-0.267815651832061,
330.087136418631));
#25031=CARTESIAN_POINT('Ctrl Pts',(7.41095176013556,-0.404358136988321,
330.098400510083));
#25032=CARTESIAN_POINT('Ctrl Pts',(7.40319270047437,-0.540765121461374,
330.109653423388));
#25033=CARTESIAN_POINT('Ctrl Pts',(7.39543364081317,-0.676844133303198,
330.126616497821));
#25034=CARTESIAN_POINT('Ctrl Pts',(7.38767458115197,-0.812081267898217,
330.149257059292));
#25035=CARTESIAN_POINT('Ctrl Pts',(7.37992136866472,-0.947216488719585,
330.171880558992));
#25036=CARTESIAN_POINT('Ctrl Pts',(7.37216815617745,-1.08151071128066,330.200172965249));
#25037=CARTESIAN_POINT('Ctrl Pts',(7.36441494369021,-1.21445535861207,330.234049806761));
#25038=CARTESIAN_POINT('Ctrl Pts',(7.3566650323184,-1.34734340158386,330.267912224398));
#25039=CARTESIAN_POINT('Ctrl Pts',(7.34891512094654,-1.4788826343657,330.307354251804));
#25040=CARTESIAN_POINT('Ctrl Pts',(7.34116520957474,-1.60857509649862,330.352240408388));
#25041=CARTESIAN_POINT('Ctrl Pts',(7.33341692158451,-1.73824039182361,330.397117162623));
#25042=CARTESIAN_POINT('Ctrl Pts',(7.32566863359428,-1.8660593169516,330.447435649982));
#25043=CARTESIAN_POINT('Ctrl Pts',(7.31792034560405,-1.9915498719978,330.503010766096));
#25044=CARTESIAN_POINT('Ctrl Pts',(7.31017200497487,-2.11704127957955,330.558586259767));
#25045=CARTESIAN_POINT('Ctrl Pts',(7.3024236643457,-2.24020392824123,330.619418295232));
#25046=CARTESIAN_POINT('Ctrl Pts',(7.29467532371652,-2.36057694154306,330.68527410308));
#25047=CARTESIAN_POINT('Ctrl Pts',(7.28692525475024,-2.48097680512852,330.751144600658));
#25048=CARTESIAN_POINT('Ctrl Pts',(7.27917518578401,-2.59858545240846,330.822040912983));
#25049=CARTESIAN_POINT('Ctrl Pts',(7.27142511681774,-2.71296804983267,330.897685114099));
#25050=CARTESIAN_POINT('Ctrl Pts',(7.26366685078835,-2.82747162700243,330.973409322282));
#25051=CARTESIAN_POINT('Ctrl Pts',(7.25590858475895,-2.93874201184566,331.053891234774));
#25052=CARTESIAN_POINT('Ctrl Pts',(7.24815031872956,-3.04637429115085,331.138810191053));
#25053=CARTESIAN_POINT('Ctrl Pts',(7.24038792079743,-3.15406389333046,331.22377437353));
#25054=CARTESIAN_POINT('Ctrl Pts',(7.23262552286524,-3.25811123289397,331.31318005398));
#25055=CARTESIAN_POINT('Ctrl Pts',(7.22486312493311,-3.35814653861724,331.406667996459));
#25056=CARTESIAN_POINT('Ctrl Pts',(7.21708834555284,-3.45834140611,331.500305057306));
#25057=CARTESIAN_POINT('Ctrl Pts',(7.20931356617262,-3.55451117760251,331.598037113311));
#25058=CARTESIAN_POINT('Ctrl Pts',(7.20153878679236,-3.64632422870232,331.699469333323));
#25059=CARTESIAN_POINT('Ctrl Pts',(7.19414020866709,-3.73369468621071,331.795993513298));
#25060=CARTESIAN_POINT('Ctrl Pts',(7.18674163054182,-3.81711998063126,331.895867948561));
#25061=CARTESIAN_POINT('Ctrl Pts',(7.17934305241656,-3.89635070610417,331.998727896784));
#25062=CARTESIAN_POINT('Ctrl Pts',(7.17155910472168,-3.97970832056288,332.106945508779));
#25063=CARTESIAN_POINT('Ctrl Pts',(7.16377515702676,-4.05868905964504,332.218813772232));
#25064=CARTESIAN_POINT('Ctrl Pts',(7.15599120933189,-4.13295648073021,332.333944150831));
#25065=CARTESIAN_POINT('Ctrl Pts',(7.14821668385917,-4.20713400345435,332.448935167753));
#25066=CARTESIAN_POINT('Ctrl Pts',(7.14044215838654,-4.27660934838268,332.56718012173));
#25067=CARTESIAN_POINT('Ctrl Pts',(7.13266763291381,-4.34108626003702,332.688257552101));
#25068=CARTESIAN_POINT('Ctrl Pts',(7.12490085180615,-4.40549894491065,332.809214374748));
#25069=CARTESIAN_POINT('Ctrl Pts',(7.11713407069846,-4.46492292106192,332.932997719246));
#25070=CARTESIAN_POINT('Ctrl Pts',(7.10936728959081,-4.51910542188317,333.059157593104));
#25071=CARTESIAN_POINT('Ctrl Pts',(7.10160658069208,-4.57324556185245,333.185218832907));
#25072=CARTESIAN_POINT('Ctrl Pts',(7.09384587179335,-4.62215222859229,333.313652548546));
#25073=CARTESIAN_POINT('Ctrl Pts',(7.08608516289462,-4.66561895164036,333.443984942041));
#25074=CARTESIAN_POINT('Ctrl Pts',(7.07832857773713,-4.7090625781491,333.574248081932));
#25075=CARTESIAN_POINT('Ctrl Pts',(7.0705719925796,-4.74707189055904,333.706407523644));
#25076=CARTESIAN_POINT('Ctrl Pts',(7.06281540742211,-4.77948897741175,333.839970613605));
#25077=CARTESIAN_POINT('Ctrl Pts',(7.05506139088635,-4.81189532922681,333.973489473657));
#25078=CARTESIAN_POINT('Ctrl Pts',(7.0473073743506,-4.83871305151345,334.108410678542));
#25079=CARTESIAN_POINT('Ctrl Pts',(7.03955335781484,-4.85983453256771,334.2442279586));
#25080=CARTESIAN_POINT('Ctrl Pts',(7.03179833874714,-4.8809587444595,334.380062798738));
#25081=CARTESIAN_POINT('Ctrl Pts',(7.02404331967943,-4.89638517703035,334.516793561927));
#25082=CARTESIAN_POINT('Ctrl Pts',(7.01628830061173,-4.90605763941331,334.653905357952));
#25083=CARTESIAN_POINT('Ctrl Pts',(7.00970428323788,-4.91426956769117,334.770313382137));
#25084=CARTESIAN_POINT('Ctrl Pts',(7.00312026586403,-4.91833488291597,334.886995785808));
#25085=CARTESIAN_POINT('Ctrl Pts',(6.99653624849017,-4.9182486560913,335.003635843242));
#25086=CARTESIAN_POINT('',(10.4965362484546,-4.91824948156304,334.997741769529));
#25087=CARTESIAN_POINT('Ctrl Pts',(10.4965362484546,-4.91824948156304,334.997741769529));
#25088=CARTESIAN_POINT('Ctrl Pts',(10.4888471502769,-4.91831149438634,335.132800852283));
#25089=CARTESIAN_POINT('Ctrl Pts',(10.4811580520993,-4.91280606153683,335.268086508271));
#25090=CARTESIAN_POINT('Ctrl Pts',(10.4734689539216,-4.90170348255283,335.403095561411));
#25091=CARTESIAN_POINT('Ctrl Pts',(10.4657887887527,-4.89061380227713,335.537947764292));
#25092=CARTESIAN_POINT('Ctrl Pts',(10.4581086235838,-4.87393994179174,335.672523608465));
#25093=CARTESIAN_POINT('Ctrl Pts',(10.4504284584148,-4.85170419160826,335.806318485234));
#25094=CARTESIAN_POINT('Ctrl Pts',(10.442755282694,-4.82948867739849,335.939991599995));
#25095=CARTESIAN_POINT('Ctrl Pts',(10.435082106973,-4.80172140816308,336.072884768922));
#25096=CARTESIAN_POINT('Ctrl Pts',(10.4274089312521,-4.76847655892465,336.204497558937));
#25097=CARTESIAN_POINT('Ctrl Pts',(10.4195986186762,-4.73463754968828,336.338462564614));
#25098=CARTESIAN_POINT('Ctrl Pts',(10.4117883061003,-4.69512331937017,336.47110056669));
#25099=CARTESIAN_POINT('Ctrl Pts',(10.4039779935244,-4.65006680406456,336.601893186276));
#25100=CARTESIAN_POINT('Ctrl Pts',(10.3963121106908,-4.60584348215994,336.730267164588));
#25101=CARTESIAN_POINT('Ctrl Pts',(10.3886462278573,-4.55628122659596,336.856863030108));
#25102=CARTESIAN_POINT('Ctrl Pts',(10.3809803450237,-4.50155618192456,336.981205442017));
#25103=CARTESIAN_POINT('Ctrl Pts',(10.3733151953191,-4.44683637089871,337.105535962403));
#25104=CARTESIAN_POINT('Ctrl Pts',(10.3656500456145,-4.3869549137158,337.227613091595));
#25105=CARTESIAN_POINT('Ctrl Pts',(10.3579848959099,-4.32213588798339,337.346981982953));
#25106=CARTESIAN_POINT('Ctrl Pts',(10.3503187339676,-4.25730830243618,337.466366637825));
#25107=CARTESIAN_POINT('Ctrl Pts',(10.3426525720253,-4.18754204271593,337.583041992139));
#25108=CARTESIAN_POINT('Ctrl Pts',(10.3349864100829,-4.11310661810113,337.696578760324));
#25109=CARTESIAN_POINT('Ctrl Pts',(10.3270676616952,-4.03621867820436,337.813856363743));
#25110=CARTESIAN_POINT('Ctrl Pts',(10.3191489133075,-3.95434884352145,337.927784611801));
#25111=CARTESIAN_POINT('Ctrl Pts',(10.3112301649197,-3.867841204291,338.03792486426));
#25112=CARTESIAN_POINT('Ctrl Pts',(10.3035526386729,-3.78396877417725,338.144710007275));
#25113=CARTESIAN_POINT('Ctrl Pts',(10.2958751124261,-3.69573728881549,338.24793430924));
#25114=CARTESIAN_POINT('Ctrl Pts',(10.2881975861793,-3.60349921123578,338.347234156303));
#25115=CARTESIAN_POINT('Ctrl Pts',(10.2801582267211,-3.50691405638744,338.45121389392));
#25116=CARTESIAN_POINT('Ctrl Pts',(10.2721188672629,-3.40593582994268,338.550889908336));
#25117=CARTESIAN_POINT('Ctrl Pts',(10.2640795078046,-3.30100881357484,338.645891369089));
#25118=CARTESIAN_POINT('Ctrl Pts',(10.2560401483464,-3.19608179720701,338.740892829843));
#25119=CARTESIAN_POINT('Ctrl Pts',(10.2480007888882,-3.08720642071983,338.831219479815));
#25120=CARTESIAN_POINT('Ctrl Pts',(10.23996142943,-2.97486136344552,338.916552429214));
#25121=CARTESIAN_POINT('Ctrl Pts',(10.2321863547283,-2.86620952156538,338.999080155401));
#25122=CARTESIAN_POINT('Ctrl Pts',(10.2244112800266,-2.7539491960901,339.077213585137));
#25123=CARTESIAN_POINT('Ctrl Pts',(10.2166362053249,-2.63847135919566,339.150620670358));
#25124=CARTESIAN_POINT('Ctrl Pts',(10.2088706983503,-2.52313562517027,339.223937423462));
#25125=CARTESIAN_POINT('Ctrl Pts',(10.2011051913756,-2.40459058441866,339.292539196675));
#25126=CARTESIAN_POINT('Ctrl Pts',(10.193339684401,-2.28325963898628,339.356134580506));
#25127=CARTESIAN_POINT('Ctrl Pts',(10.1855818769466,-2.16204899350117,339.419666909348));
#25128=CARTESIAN_POINT('Ctrl Pts',(10.1778240694924,-2.0380582843033,339.478202546856));
#25129=CARTESIAN_POINT('Ctrl Pts',(10.170066262038,-1.91173890797882,339.531493949044));
#25130=CARTESIAN_POINT('Ctrl Pts',(10.1623142925723,-1.78551459086761,339.584745247814));
#25131=CARTESIAN_POINT('Ctrl Pts',(10.1545623231064,-1.65696545337093,339.632760015154));
#25132=CARTESIAN_POINT('Ctrl Pts',(10.1468103536407,-1.52656612983506,339.675337304809));
#25133=CARTESIAN_POINT('Ctrl Pts',(10.1390616671101,-1.39622203001107,339.717896563114));
#25134=CARTESIAN_POINT('Ctrl Pts',(10.1313129805795,-1.26402967336585,339.75502280268));
#25135=CARTESIAN_POINT('Ctrl Pts',(10.1235642940489,-1.1304820432802,339.786563841872));
#25136=CARTESIAN_POINT('Ctrl Pts',(10.1158172196792,-0.996962198582865,
339.818098318762));
#25137=CARTESIAN_POINT('Ctrl Pts',(10.1080701453095,-0.862088021479138,
339.844049816859));
#25138=CARTESIAN_POINT('Ctrl Pts',(10.1003230709398,-0.726365585908918,
339.864316611623));
#25139=CARTESIAN_POINT('Ctrl Pts',(10.0925759316195,-0.590642012457482,
339.884583576301));
#25140=CARTESIAN_POINT('Ctrl Pts',(10.0848287922992,-0.454070552943152,
339.899165684858));
#25141=CARTESIAN_POINT('Ctrl Pts',(10.077081652979,-0.317164960868917,339.908012780148));
#25142=CARTESIAN_POINT('Ctrl Pts',(10.0693327719101,-0.180228589030351,
339.916861864485));
#25143=CARTESIAN_POINT('Ctrl Pts',(10.0615838908412,-0.0429583251338626,
339.919973344645));
#25144=CARTESIAN_POINT('Ctrl Pts',(10.0538350097723,0.0941298975525665,
339.917349146124));
#25145=CARTESIAN_POINT('Ctrl Pts',(10.0460779038931,0.231363628296001,339.914722162228));
#25146=CARTESIAN_POINT('Ctrl Pts',(10.038320798014,0.368414540429873,339.906347345875));
#25147=CARTESIAN_POINT('Ctrl Pts',(10.0305636921348,0.504769091797421,339.892278735565));
#25148=CARTESIAN_POINT('Ctrl Pts',(10.0228024410756,0.64119650721525,339.878202607385));
#25149=CARTESIAN_POINT('Ctrl Pts',(10.0150411900165,0.776926433798234,339.858426678913));
#25150=CARTESIAN_POINT('Ctrl Pts',(10.0072799389574,0.911454362244702,339.833056383702));
#25151=CARTESIAN_POINT('Ctrl Pts',(9.99950627233217,1.0461974931591,339.807645503981));
#25152=CARTESIAN_POINT('Ctrl Pts',(9.99173260570696,1.17973440263807,339.776622462804));
#25153=CARTESIAN_POINT('Ctrl Pts',(9.98395893908176,1.31157374575264,339.740143180533));
#25154=CARTESIAN_POINT('Ctrl Pts',(9.97654709110647,1.43727673964733,339.705361795187));
#25155=CARTESIAN_POINT('Ctrl Pts',(9.96913524313119,1.56143636007777,339.665620737365));
#25156=CARTESIAN_POINT('Ctrl Pts',(9.9617233951559,1.68364446007505,339.621095583794));
#25157=CARTESIAN_POINT('Ctrl Pts',(9.95394831592372,1.81184159302493,339.574388393091));
#25158=CARTESIAN_POINT('Ctrl Pts',(9.94617323669155,1.93829622334815,339.52226874059));
#25159=CARTESIAN_POINT('Ctrl Pts',(9.93839815745937,2.06251754688526,339.464885713128));
#25160=CARTESIAN_POINT('Ctrl Pts',(9.93063264598798,2.18658600768336,339.407573299361));
#25161=CARTESIAN_POINT('Ctrl Pts',(9.92286713451661,2.30842627844374,339.345010560234));
#25162=CARTESIAN_POINT('Ctrl Pts',(9.91510162304522,2.42756417920079,339.277395845414));
#25163=CARTESIAN_POINT('Ctrl Pts',(9.90734381113198,2.54658395390795,339.209848171049));
#25164=CARTESIAN_POINT('Ctrl Pts',(9.89958599921864,2.66290635305307,339.137258681006));
#25165=CARTESIAN_POINT('Ctrl Pts',(9.89182818730541,2.77607893466425,339.059873004296));
#25166=CARTESIAN_POINT('Ctrl Pts',(9.88407621342275,2.88916634986523,338.982545563073));
#25167=CARTESIAN_POINT('Ctrl Pts',(9.87632423954012,2.99910834424228,338.90042933906));
#25168=CARTESIAN_POINT('Ctrl Pts',(9.86857226565746,3.10547908556348,338.813814719101));
#25169=CARTESIAN_POINT('Ctrl Pts',(9.86082357478872,3.21180477814875,338.727236781025));
#25170=CARTESIAN_POINT('Ctrl Pts',(9.85307488392002,3.31456192336565,338.636164482408));
#25171=CARTESIAN_POINT('Ctrl Pts',(9.84532619305128,3.41335576647654,338.540930029521));
#25172=CARTESIAN_POINT('Ctrl Pts',(9.83757911439184,3.5121290543278,338.445715391318));
#25173=CARTESIAN_POINT('Ctrl Pts',(9.82983203573236,3.60694039905087,338.346340592457));
#25174=CARTESIAN_POINT('Ctrl Pts',(9.82208495707292,3.6974303922948,338.243176152576));
#25175=CARTESIAN_POINT('Ctrl Pts',(9.81433781351512,3.78792114358594,338.140010848471));
#25176=CARTESIAN_POINT('Ctrl Pts',(9.80659066995731,3.87409021344412,338.033056133875));
#25177=CARTESIAN_POINT('Ctrl Pts',(9.79884352639951,3.95561740177701,337.922716892424));
#25178=CARTESIAN_POINT('Ctrl Pts',(9.79109464114915,4.03716291883921,337.812352844792));
#25179=CARTESIAN_POINT('Ctrl Pts',(9.78334575589884,4.11406424554177,337.698603070507));
#25180=CARTESIAN_POINT('Ctrl Pts',(9.77559687064849,4.18604379958458,337.581902471136));
#25181=CARTESIAN_POINT('Ctrl Pts',(9.76783976069935,4.25809975302312,337.465078005268));
#25182=CARTESIAN_POINT('Ctrl Pts',(9.76008265075019,4.32522329287327,337.345296791023));
#25183=CARTESIAN_POINT('Ctrl Pts',(9.75232554080105,4.38718195373206,337.223019920592));
#25184=CARTESIAN_POINT('Ctrl Pts',(9.74456428572623,4.44917372311168,337.100677709718));
#25185=CARTESIAN_POINT('Ctrl Pts',(9.73680303065142,4.50599495225126,336.975837540934));
#25186=CARTESIAN_POINT('Ctrl Pts',(9.7290417755766,4.5574612831223,336.848980723356));
#25187=CARTESIAN_POINT('Ctrl Pts',(9.72126810506841,4.6090099430491,336.721920976953));
#25188=CARTESIAN_POINT('Ctrl Pts',(9.71349443456021,4.6551864554554,336.592838503541));
#25189=CARTESIAN_POINT('Ctrl Pts',(9.70572076405202,4.69585604173562,336.462230863371));
#25190=CARTESIAN_POINT('Ctrl Pts',(9.69830896299535,4.73463243214838,336.337703094359));
#25191=CARTESIAN_POINT('Ctrl Pts',(9.6908971619387,4.76840298317807,336.211789235325));
#25192=CARTESIAN_POINT('Ctrl Pts',(9.68348536088203,4.79709447026861,336.084927511781));
#25193=CARTESIAN_POINT('Ctrl Pts',(9.67571026849582,4.8271922779568,335.951847628322));
#25194=CARTESIAN_POINT('Ctrl Pts',(9.66793517610962,4.85179564187078,335.817304059386));
#25195=CARTESIAN_POINT('Ctrl Pts',(9.66016008372341,4.87076433084771,335.681790213953));
#25196=CARTESIAN_POINT('Ctrl Pts',(9.65239455901105,4.8897096778217,335.546443125672));
#25197=CARTESIAN_POINT('Ctrl Pts',(9.64462903429864,4.90303409241489,335.410128519967));
#25198=CARTESIAN_POINT('Ctrl Pts',(9.63686350958628,4.91064776597322,335.273352484975));
#25199=CARTESIAN_POINT('Ctrl Pts',(9.62910568435987,4.91825389060538,335.136712062863));
#25200=CARTESIAN_POINT('Ctrl Pts',(9.62134785913349,4.92016052067019,334.999611509679));
#25201=CARTESIAN_POINT('Ctrl Pts',(9.61359003390709,4.91632936941955,334.862564219059));
#25202=CARTESIAN_POINT('Ctrl Pts',(9.60583804665353,4.91250110121362,334.725620060224));
#25203=CARTESIAN_POINT('Ctrl Pts',(9.59808605939994,4.90294365701153,334.588729473318));
#25204=CARTESIAN_POINT('Ctrl Pts',(9.59033407214639,4.88767078794349,334.452407696197));
#25205=CARTESIAN_POINT('Ctrl Pts',(9.58258536786679,4.87240438694997,334.316143651478));
#25206=CARTESIAN_POINT('Ctrl Pts',(9.57483666358718,4.8514274186996,334.180448325063));
#25207=CARTESIAN_POINT('Ctrl Pts',(9.56708795930757,4.82480561898035,334.045833451878));
#25208=CARTESIAN_POINT('Ctrl Pts',(9.55934086721488,4.79818935816356,333.911246586516));
#25209=CARTESIAN_POINT('Ctrl Pts',(9.55159377512222,4.76593067774082,333.777740110451));
#25210=CARTESIAN_POINT('Ctrl Pts',(9.54384668302953,4.72814665997359,333.645816768572));
#25211=CARTESIAN_POINT('Ctrl Pts',(9.53609952602892,4.69036232563831,333.513892321392));
#25212=CARTESIAN_POINT('Ctrl Pts',(9.52835236902829,4.64705266924542,333.383551410618));
#25213=CARTESIAN_POINT('Ctrl Pts',(9.52060521202768,4.59838488829934,333.255282406359));
#25214=CARTESIAN_POINT('Ctrl Pts',(9.5128563133378,4.54970616602966,333.126984565102));
#25215=CARTESIAN_POINT('Ctrl Pts',(9.50510741464794,4.49566706082928,333.000759922629));
#25216=CARTESIAN_POINT('Ctrl Pts',(9.49735851595807,4.43648307584502,332.877077255235));
#25217=CARTESIAN_POINT('Ctrl Pts',(9.48960139265084,4.37723627346574,332.753263312075));
#25218=CARTESIAN_POINT('Ctrl Pts',(9.48184426934362,4.31283385195929,332.631997086707));
#25219=CARTESIAN_POINT('Ctrl Pts',(9.4740871460364,4.24353775405405,332.513723588895));
#25220=CARTESIAN_POINT('Ctrl Pts',(9.46632587762673,4.17420462703208,332.395386890364));
#25221=CARTESIAN_POINT('Ctrl Pts',(9.45856460921701,4.09997282444036,332.28004643445));
#25222=CARTESIAN_POINT('Ctrl Pts',(9.45080334080734,4.02114732351632,332.168117716946));
#25223=CARTESIAN_POINT('Ctrl Pts',(9.44302965713918,3.94219572993343,332.056009953455));
#25224=CARTESIAN_POINT('Ctrl Pts',(9.43525597347108,3.85863599234976,331.94732514424));
#25225=CARTESIAN_POINT('Ctrl Pts',(9.42748228980292,3.77081358420248,331.842445887131));
#25226=CARTESIAN_POINT('Ctrl Pts',(9.42007063540466,3.68708116526223,331.742450976041));
#25227=CARTESIAN_POINT('Ctrl Pts',(9.41265898100637,3.59947436273894,331.645915354763));
#25228=CARTESIAN_POINT('Ctrl Pts',(9.40524732660811,3.50832204309355,331.553137730567));
#25229=CARTESIAN_POINT('Ctrl Pts',(9.39747227725628,3.41270050629583,331.455811200198));
#25230=CARTESIAN_POINT('Ctrl Pts',(9.38969722790442,3.31287480120373,331.362312928328));
#25231=CARTESIAN_POINT('Ctrl Pts',(9.3819221785526,3.2091839533473,331.273027848765));
#25232=CARTESIAN_POINT('Ctrl Pts',(9.37415669693203,3.10562070418771,331.183852640614));
#25233=CARTESIAN_POINT('Ctrl Pts',(9.36639121531147,2.99820206935068,331.098880561473));
#25234=CARTESIAN_POINT('Ctrl Pts',(9.3586257336909,2.88730502329413,331.01846100547));
#25235=CARTESIAN_POINT('Ctrl Pts',(9.35086795156883,2.77651793199397,330.9381211857));
#25236=CARTESIAN_POINT('Ctrl Pts',(9.34311016944679,2.6622596072842,330.862325134263));
#25237=CARTESIAN_POINT('Ctrl Pts',(9.33535238732472,2.54494104864929,330.791382873033));
#25238=CARTESIAN_POINT('Ctrl Pts',(9.32760044314372,2.42771077540587,330.720493997775));
#25239=CARTESIAN_POINT('Ctrl Pts',(9.31984849896273,2.30742518519683,330.654451843832));
#25240=CARTESIAN_POINT('Ctrl Pts',(9.31209655478173,2.18452498922378,330.593523671463));
#25241=CARTESIAN_POINT('Ctrl Pts',(9.30434789337568,2.06167683873446,330.532621300812));
#25242=CARTESIAN_POINT('Ctrl Pts',(9.29659923196962,1.93621663415238,330.476828777653));
#25243=CARTESIAN_POINT('Ctrl Pts',(9.28885057056357,1.80861027304298,330.426367751694));
#25244=CARTESIAN_POINT('Ctrl Pts',(9.28110352121754,1.68103045963037,330.375917223833));
#25245=CARTESIAN_POINT('Ctrl Pts',(9.27335647187147,1.55130574105981,330.330796130575));
#25246=CARTESIAN_POINT('Ctrl Pts',(9.26560942252544,1.41992224160266,330.291178078298));
#25247=CARTESIAN_POINT('Ctrl Pts',(9.25786230810484,1.28853763853482,330.251559693232));
#25248=CARTESIAN_POINT('Ctrl Pts',(9.25011519368424,1.15549460102207,330.217444554194));
#25249=CARTESIAN_POINT('Ctrl Pts',(9.24236807926363,1.02129428555199,330.188956345573));
#25250=CARTESIAN_POINT('Ctrl Pts',(9.23461922294723,0.887063795883884,330.160461731537));
#25251=CARTESIAN_POINT('Ctrl Pts',(9.22687036663084,0.75167589275711,330.137596646645));
#25252=CARTESIAN_POINT('Ctrl Pts',(9.21912151031444,0.615641396738061,330.120433550701));
#25253=CARTESIAN_POINT('Ctrl Pts',(9.21136442881664,0.479462504131856,330.103252236639));
#25254=CARTESIAN_POINT('Ctrl Pts',(9.20360734731886,0.342636036022161,330.091785050952));
#25255=CARTESIAN_POINT('Ctrl Pts',(9.19585026582106,0.205677958286601,330.086052539966));
#25256=CARTESIAN_POINT('Ctrl Pts',(9.18808903897985,0.0686466908771019,
330.080316965556));
#25257=CARTESIAN_POINT('Ctrl Pts',(9.18032781213862,-0.0685159356209527,
330.080322172283));
#25258=CARTESIAN_POINT('Ctrl Pts',(9.1725665852974,-0.205295485973605,330.086036546133));
#25259=CARTESIAN_POINT('Ctrl Pts',(9.16479294236726,-0.342293850580163,
330.091760061602));
#25260=CARTESIAN_POINT('Ctrl Pts',(9.15701929943711,-0.478907524710492,
330.103210962543));
#25261=CARTESIAN_POINT('Ctrl Pts',(9.14924565650696,-0.6146278230349,330.120305777853));
#25262=CARTESIAN_POINT('Ctrl Pts',(9.14183353511603,-0.744036304416612,
330.136605580581));
#25263=CARTESIAN_POINT('Ctrl Pts',(9.13442141372511,-0.872632352247695,
330.158036102549));
#25264=CARTESIAN_POINT('Ctrl Pts',(9.12700929233418,-0.999986725793719,
330.184482415073));
#25265=CARTESIAN_POINT('Ctrl Pts',(9.11923420193379,-1.13357759876798,330.212223794334));
#25266=CARTESIAN_POINT('Ctrl Pts',(9.1114591115334,-1.26622430565804,330.245572289037));
#25267=CARTESIAN_POINT('Ctrl Pts',(9.10368402113301,-1.39741967742271,330.284451112792));
#25268=CARTESIAN_POINT('Ctrl Pts',(9.09591849865652,-1.5284536018898,330.323282092777));
#25269=CARTESIAN_POINT('Ctrl Pts',(9.08815297618008,-1.65803937366631,330.367629750723));
#25270=CARTESIAN_POINT('Ctrl Pts',(9.08038745370359,-1.78567917362964,330.417366155652));
#25271=CARTESIAN_POINT('Ctrl Pts',(9.07262963095745,-1.91319241520053,330.467053245559));
#25272=CARTESIAN_POINT('Ctrl Pts',(9.06487180821126,-2.03876316288809,330.522118308392));
#25273=CARTESIAN_POINT('Ctrl Pts',(9.05711398546512,-2.16190829377092,330.582383494256));
#25274=CARTESIAN_POINT('Ctrl Pts',(9.04936200093086,-2.28496075079552,330.642603327069));
#25275=CARTESIAN_POINT('Ctrl Pts',(9.04161001639658,-2.40559087474751,330.708015322369));
#25276=CARTESIAN_POINT('Ctrl Pts',(9.03385803186231,-2.52333542321499,330.77839350431));
#25277=CARTESIAN_POINT('Ctrl Pts',(9.0261093306521,-2.64103010141928,330.848741877836));
#25278=CARTESIAN_POINT('Ctrl Pts',(9.01836062944187,-2.75584130014947,330.924052054346));
#25279=CARTESIAN_POINT('Ctrl Pts',(9.01061192823167,-2.86733050215,331.004052195794));
#25280=CARTESIAN_POINT('Ctrl Pts',(9.00286483942059,-2.97879650476691,331.084035690303));
#25281=CARTESIAN_POINT('Ctrl Pts',(8.99511775060953,-3.08694156824916,331.168706980846));
#25282=CARTESIAN_POINT('Ctrl Pts',(8.98737066179845,-3.19135663013834,331.257751221288));
#25283=CARTESIAN_POINT('Ctrl Pts',(8.97962350828745,-3.29577256405141,331.346796205384));
#25284=CARTESIAN_POINT('Ctrl Pts',(8.97187635477651,-3.396458136826,331.440213958594));
#25285=CARTESIAN_POINT('Ctrl Pts',(8.96412920126551,-3.49303813159524,331.537649978162));
#25286=CARTESIAN_POINT('Ctrl Pts',(8.95638030626916,-3.58963983661529,331.635107900407));
#25287=CARTESIAN_POINT('Ctrl Pts',(8.9486314112728,-3.68213385206024,331.736585608859));
#25288=CARTESIAN_POINT('Ctrl Pts',(8.94088251627645,-3.77018280701602,331.84169275336));
#25289=CARTESIAN_POINT('Ctrl Pts',(8.93312539696105,-3.85832521306356,331.946911453726));
#25290=CARTESIAN_POINT('Ctrl Pts',(8.92536827764563,-3.94201288301005,332.055766984999));
#25291=CARTESIAN_POINT('Ctrl Pts',(8.91761115833023,-4.02094931658228,332.167836576753));
#25292=CARTESIAN_POINT('Ctrl Pts',(8.90984989408107,-4.09992792899377,332.279966051696));
#25293=CARTESIAN_POINT('Ctrl Pts',(8.90208862983192,-4.17415003489472,332.395312680657));
#25294=CARTESIAN_POINT('Ctrl Pts',(8.89432736558277,-4.24336382492132,332.51342675317));
#25295=CARTESIAN_POINT('Ctrl Pts',(8.8865536863183,-4.31268833019164,332.63172976243));
#25296=CARTESIAN_POINT('Ctrl Pts',(8.87878000705385,-4.37698832708292,332.752808715978));
#25297=CARTESIAN_POINT('Ctrl Pts',(8.87100632778939,-4.43605872546199,332.876190675519));
#25298=CARTESIAN_POINT('Ctrl Pts',(8.86359463787971,-4.49237845010362,332.99382722746));
#25299=CARTESIAN_POINT('Ctrl Pts',(8.85618294796999,-4.5439445387058,333.113556867035));
#25300=CARTESIAN_POINT('Ctrl Pts',(8.84877125806031,-4.59062137118073,333.234956519244));
#25301=CARTESIAN_POINT('Ctrl Pts',(8.83991442260744,-4.64639934216028,333.380026908961));
#25302=CARTESIAN_POINT('Ctrl Pts',(8.83105758715456,-4.69534296381877,333.527863253388));
#25303=CARTESIAN_POINT('Ctrl Pts',(8.8222007517017,-4.73720468645838,333.67785219393));
#25304=CARTESIAN_POINT('Ctrl Pts',(8.81337370149808,-4.77892562948784,333.827336726548));
#25305=CARTESIAN_POINT('Ctrl Pts',(8.80454665129447,-4.81361211826951,333.978959243898));
#25306=CARTESIAN_POINT('Ctrl Pts',(8.79571960109084,-4.84106555254952,334.132090224494));
#25307=CARTESIAN_POINT('Ctrl Pts',(8.7869498317336,-4.86834083490837,334.284227501421));
#25308=CARTESIAN_POINT('Ctrl Pts',(8.77818006237633,-4.88847654611716,334.437853555313));
#25309=CARTESIAN_POINT('Ctrl Pts',(8.76941029301909,-4.90132527004678,334.592331434005));
#25310=CARTESIAN_POINT('Ctrl Pts',(8.76178561152781,-4.91249630813708,334.726638799967));
#25311=CARTESIAN_POINT('Ctrl Pts',(8.75416093003657,-4.91815974619261,334.861589698482));
#25312=CARTESIAN_POINT('Ctrl Pts',(8.74653624854528,-4.91824892942493,334.996754894379));
#25313=CARTESIAN_POINT('',(12.2465362485257,-4.91824798382928,335.004453320022));
#25314=CARTESIAN_POINT('Ctrl Pts',(12.2465362484902,-4.91824798382871,335.004453320647));
#25315=CARTESIAN_POINT('Ctrl Pts',(12.2356922904606,-4.9180747842582,335.195734952039));
#25316=CARTESIAN_POINT('Ctrl Pts',(12.2248483324311,-4.90673912433975,335.38653135153));
#25317=CARTESIAN_POINT('Ctrl Pts',(12.2140043744016,-4.8844305574504,335.575778769967));
#25318=CARTESIAN_POINT('Ctrl Pts',(12.2052121393835,-4.86634286636259,335.729219771392));
#25319=CARTESIAN_POINT('Ctrl Pts',(12.1964199043656,-4.84104259945817,335.881643403505));
#25320=CARTESIAN_POINT('Ctrl Pts',(12.1876276693475,-4.80865222242309,336.032495455818));
#25321=CARTESIAN_POINT('Ctrl Pts',(12.1798525905152,-4.78000902369811,336.165895734173));
#25322=CARTESIAN_POINT('Ctrl Pts',(12.1720775116828,-4.7457652275205,336.298313990164));
#25323=CARTESIAN_POINT('Ctrl Pts',(12.1643024328504,-4.706001044865,336.429243586038));
#25324=CARTESIAN_POINT('Ctrl Pts',(12.1565369217473,-4.66628579456685,336.560012064711));
#25325=CARTESIAN_POINT('Ctrl Pts',(12.1487714106443,-4.6210637867871,336.689295157775));
#25326=CARTESIAN_POINT('Ctrl Pts',(12.1410058995412,-4.57046631275356,336.816595922732));
#25327=CARTESIAN_POINT('Ctrl Pts',(12.1332480879649,-4.51991900626218,336.943770468611));
#25328=CARTESIAN_POINT('Ctrl Pts',(12.1254902763886,-4.46400698354382,337.068966236913));
#25329=CARTESIAN_POINT('Ctrl Pts',(12.1177324648123,-4.40291135431033,337.191701318288));
#25330=CARTESIAN_POINT('Ctrl Pts',(12.1099804912352,-4.3418617014748,337.314344037624));
#25331=CARTESIAN_POINT('Ctrl Pts',(12.1022285176581,-4.27563638001457,337.434529407331));
#25332=CARTESIAN_POINT('Ctrl Pts',(12.0944765440809,-4.20446449016407,337.551795723299));
#25333=CARTESIAN_POINT('Ctrl Pts',(12.0867278534694,-4.13332274165271,337.669012376911));
#25334=CARTESIAN_POINT('Ctrl Pts',(12.0789791628578,-4.0572387936894,337.783312102087));
#25335=CARTESIAN_POINT('Ctrl Pts',(12.0712304722462,-3.97648744060711,337.894258229183));
#25336=CARTESIAN_POINT('Ctrl Pts',(12.0634833938146,-3.89575288851937,338.005181273009));
#25337=CARTESIAN_POINT('Ctrl Pts',(12.0557363153829,-3.81035309275928,338.112751790787));
#25338=CARTESIAN_POINT('Ctrl Pts',(12.0479892369513,-3.72060565573107,338.216562857623));
#25339=CARTESIAN_POINT('Ctrl Pts',(12.0402420935918,-3.63085746653497,338.320374794494));
#25340=CARTESIAN_POINT('Ctrl Pts',(12.0324949502323,-3.53676181902775,338.420426921884));
#25341=CARTESIAN_POINT('Ctrl Pts',(12.0247478068729,-3.43867574261208,338.51634642771));
#25342=CARTESIAN_POINT('Ctrl Pts',(12.0169989217914,-3.34056761436709,338.612287498275));
#25343=CARTESIAN_POINT('Ctrl Pts',(12.0092500367099,-3.23846755142362,338.704093825234));
#25344=CARTESIAN_POINT('Ctrl Pts',(12.0015011516284,-3.13276817400756,338.791430683848));
#25345=CARTESIAN_POINT('Ctrl Pts',(11.9937440418009,-3.02695660618964,338.878860242699));
#25346=CARTESIAN_POINT('Ctrl Pts',(11.9859869319734,-2.91753839419017,338.961810607373));
#25347=CARTESIAN_POINT('Ctrl Pts',(11.9782298221459,-2.80493830157268,339.039988141922));
#25348=CARTESIAN_POINT('Ctrl Pts',(11.9704685671672,-2.69227803907027,339.118207452043));
#25349=CARTESIAN_POINT('Ctrl Pts',(11.9627073121885,-2.57643283791569,339.191648640863));
#25350=CARTESIAN_POINT('Ctrl Pts',(11.9549460572098,-2.45785409904911,339.260062944404));
#25351=CARTESIAN_POINT('Ctrl Pts',(11.9471723867536,-2.33908567286134,339.328586688526));
#25352=CARTESIAN_POINT('Ctrl Pts',(11.9393987162974,-2.21757531750122,339.392067297226));
#25353=CARTESIAN_POINT('Ctrl Pts',(11.9316250458413,-2.09379734547272,339.450302881669));
#25354=CARTESIAN_POINT('Ctrl Pts',(11.9242132422521,-1.97578127796429,339.505827580873));
#25355=CARTESIAN_POINT('Ctrl Pts',(11.9168014386628,-1.85570422332627,339.556584467194));
#25356=CARTESIAN_POINT('Ctrl Pts',(11.9093896350736,-1.73399018350044,339.602440777025));
#25357=CARTESIAN_POINT('Ctrl Pts',(11.9016145563667,-1.60631056706227,339.650544644573));
#25358=CARTESIAN_POINT('Ctrl Pts',(11.8938394776597,-1.47642594956655,339.693407421766));
#25359=CARTESIAN_POINT('Ctrl Pts',(11.8860643989528,-1.3448057802539,339.730822388961));
#25360=CARTESIAN_POINT('Ctrl Pts',(11.8782988879751,-1.21334757793775,339.768191314658));
#25361=CARTESIAN_POINT('Ctrl Pts',(11.8705333769974,-1.08015844563361,339.800125663294));
#25362=CARTESIAN_POINT('Ctrl Pts',(11.8627678660198,-0.94572732209144,339.826466916363));
#25363=CARTESIAN_POINT('Ctrl Pts',(11.8550100545687,-0.811429487396761,
339.852782052004));
#25364=CARTESIAN_POINT('Ctrl Pts',(11.8472522431175,-0.67589249320408,339.873515053399));
#25365=CARTESIAN_POINT('Ctrl Pts',(11.8394944316664,-0.539619596209107,
339.888557430765));
#25366=CARTESIAN_POINT('Ctrl Pts',(11.8317424582142,-0.403449248886334,
339.903588488266));
#25367=CARTESIAN_POINT('Ctrl Pts',(11.8239904847621,-0.266544488003686,
339.912937402883));
#25368=CARTESIAN_POINT('Ctrl Pts',(11.8162385113098,-0.129417549668234,
339.916546975301));
#25369=CARTESIAN_POINT('Ctrl Pts',(11.8084898208223,0.00765131533958613,
339.920155019063));
#25370=CARTESIAN_POINT('Ctrl Pts',(11.8007411303348,0.144941780731573,339.918028544682));
#25371=CARTESIAN_POINT('Ctrl Pts',(11.7929924398473,0.281937934718363,339.910162325572));
#25372=CARTESIAN_POINT('Ctrl Pts',(11.7852453615391,0.418905585518681,339.902297743094));
#25373=CARTESIAN_POINT('Ctrl Pts',(11.7774982832308,0.555578656725884,339.88869581363));
#25374=CARTESIAN_POINT('Ctrl Pts',(11.7697512049226,0.691443083642843,339.869403405406));
#25375=CARTESIAN_POINT('Ctrl Pts',(11.762004061686,0.827308649243271,339.850110835492));
#25376=CARTESIAN_POINT('Ctrl Pts',(11.7542569184493,0.962365170043431,339.825127746644));
#25377=CARTESIAN_POINT('Ctrl Pts',(11.7465097752126,1.09610593132346,339.794552622489));
#25378=CARTESIAN_POINT('Ctrl Pts',(11.7387608902531,1.22987676037613,339.763970624395));
#25379=CARTESIAN_POINT('Ctrl Pts',(11.7310120052936,1.36233086030921,339.727794176385));
#25380=CARTESIAN_POINT('Ctrl Pts',(11.7232631203341,1.49297428462808,339.686172302417));
#25381=CARTESIAN_POINT('Ctrl Pts',(11.7155060106266,1.62375637525008,339.644506250555));
#25382=CARTESIAN_POINT('Ctrl Pts',(11.7077489009192,1.75272357812367,339.597383345817));
#25383=CARTESIAN_POINT('Ctrl Pts',(11.6999917912118,1.87939910459171,339.545001877685));
#25384=CARTESIAN_POINT('Ctrl Pts',(11.6922305363523,2.00614232242113,339.492592418567));
#25385=CARTESIAN_POINT('Ctrl Pts',(11.6844692814928,2.13059106925939,339.434918961127));
#25386=CARTESIAN_POINT('Ctrl Pts',(11.6767080266333,2.25229187523389,339.37222647758));
#25387=CARTESIAN_POINT('Ctrl Pts',(11.6689343562937,2.37418736286358,339.309433706478));
#25388=CARTESIAN_POINT('Ctrl Pts',(11.6611606859541,2.49332578563743,339.241606058823));
#25389=CARTESIAN_POINT('Ctrl Pts',(11.6533870156144,2.60928069322757,339.169033140484));
#25390=CARTESIAN_POINT('Ctrl Pts',(11.6459752106761,2.71983788425184,339.099838501267));
#25391=CARTESIAN_POINT('Ctrl Pts',(11.6385634057378,2.82750103706588,339.026330595297));
#25392=CARTESIAN_POINT('Ctrl Pts',(11.6311516007995,2.93192905595593,338.948794129015));
#25393=CARTESIAN_POINT('Ctrl Pts',(11.6233765220673,3.04147539122533,338.867457378388));
#25394=CARTESIAN_POINT('Ctrl Pts',(11.6156014433349,3.14780763439471,338.781430140587));
#25395=CARTESIAN_POINT('Ctrl Pts',(11.6078263646027,3.25049790458387,338.690995317634));
#25396=CARTESIAN_POINT('Ctrl Pts',(11.6000608536006,3.35306180784718,338.600671780497));
#25397=CARTESIAN_POINT('Ctrl Pts',(11.5922953425986,3.45199236485349,338.505951705905));
#25398=CARTESIAN_POINT('Ctrl Pts',(11.5845298315965,3.54689168119188,338.407160469422));
#25399=CARTESIAN_POINT('Ctrl Pts',(11.576772020122,3.64169690457268,338.308467184747));
#25400=CARTESIAN_POINT('Ctrl Pts',(11.5690142086474,3.73247857247892,338.205711051252));
#25401=CARTESIAN_POINT('Ctrl Pts',(11.5612563971729,3.8188731124596,338.099256558182));
#25402=CARTESIAN_POINT('Ctrl Pts',(11.5535044236981,3.90520263780165,337.992882175503));
#25403=CARTESIAN_POINT('Ctrl Pts',(11.5457524502234,3.98715136128012,337.882815275219));
#25404=CARTESIAN_POINT('Ctrl Pts',(11.5380004767486,4.06439398241709,337.769455653769));
#25405=CARTESIAN_POINT('Ctrl Pts',(11.5302517862401,4.14160389124996,337.656144040197));
#25406=CARTESIAN_POINT('Ctrl Pts',(11.5225030957316,4.21411144211037,337.539542801303));
#25407=CARTESIAN_POINT('Ctrl Pts',(11.514754405223,4.28163305037375,337.42008294991));
#25408=CARTESIAN_POINT('Ctrl Pts',(11.5070073268947,4.34914061019844,337.300647953145));
#25409=CARTESIAN_POINT('Ctrl Pts',(11.4992602485664,4.41166409860948,337.178355866962));
#25410=CARTESIAN_POINT('Ctrl Pts',(11.4915131702381,4.46896473818857,337.05366434242));
#25411=CARTESIAN_POINT('Ctrl Pts',(11.4837660269823,4.52626585799893,336.92897177285));
#25412=CARTESIAN_POINT('Ctrl Pts',(11.4760188837265,4.57834387845695,336.801880079977));
#25413=CARTESIAN_POINT('Ctrl Pts',(11.4682717404706,4.62500740413147,336.672868666163));
#25414=CARTESIAN_POINT('Ctrl Pts',(11.4605228554929,4.67168142075504,336.54382824785));
#25415=CARTESIAN_POINT('Ctrl Pts',(11.4527739705152,4.71293838739378,336.412867617268));
#25416=CARTESIAN_POINT('Ctrl Pts',(11.4450250855375,4.7486363186781,336.280482789979));
#25417=CARTESIAN_POINT('Ctrl Pts',(11.4372679758134,4.7843721401144,336.14795744807));
#25418=CARTESIAN_POINT('Ctrl Pts',(11.4295108660893,4.81453703763284,336.014005267767));
#25419=CARTESIAN_POINT('Ctrl Pts',(11.4217537563652,4.83903973938198,335.87913449664));
#25420=CARTESIAN_POINT('Ctrl Pts',(11.4139925014899,4.86355553459078,335.744191654889));
#25421=CARTESIAN_POINT('Ctrl Pts',(11.4062312466147,4.88240305137542,335.60832963119));
#25422=CARTESIAN_POINT('Ctrl Pts',(11.3984699917395,4.89554289352523,335.472062326557));
#25423=CARTESIAN_POINT('Ctrl Pts',(11.3906963213856,4.90870375514054,335.335577038643));
#25424=CARTESIAN_POINT('Ctrl Pts',(11.3829226510317,4.91613867562981,335.19868556477));
#25425=CARTESIAN_POINT('Ctrl Pts',(11.3751489806778,4.91786041399784,335.06190323847));
#25426=CARTESIAN_POINT('Ctrl Pts',(11.3677371759604,4.91950200516101,334.931488152007));
#25427=CARTESIAN_POINT('Ctrl Pts',(11.3603253712431,4.91595034845745,334.801172567865));
#25428=CARTESIAN_POINT('Ctrl Pts',(11.3529135665257,4.90726027313532,334.67139739166));
#25429=CARTESIAN_POINT('Ctrl Pts',(11.3451384873979,4.89814427159027,334.535261551297));
#25430=CARTESIAN_POINT('Ctrl Pts',(11.3373634082702,4.88334460907246,334.399290217979));
#25431=CARTESIAN_POINT('Ctrl Pts',(11.3295883291424,4.86286763306565,334.263996300429));
#25432=CARTESIAN_POINT('Ctrl Pts',(11.3218228177432,4.84241585527778,334.128868870633));
#25433=CARTESIAN_POINT('Ctrl Pts',(11.3140573063439,4.81630072265831,333.994417580752));
#25434=CARTESIAN_POINT('Ctrl Pts',(11.3062917949446,4.78458052699886,333.861153108112));
#25435=CARTESIAN_POINT('Ctrl Pts',(11.2985339830716,4.75289178200195,333.728020767569));
#25436=CARTESIAN_POINT('Ctrl Pts',(11.2907761711985,4.71560912350224,333.596073280305));
#25437=CARTESIAN_POINT('Ctrl Pts',(11.2830183593254,4.67284230840082,333.465813628232));
#25438=CARTESIAN_POINT('Ctrl Pts',(11.2752663854514,4.63010767668131,333.33565200067));
#25439=CARTESIAN_POINT('Ctrl Pts',(11.2675144115773,4.58189722439204,333.207176050004));
#25440=CARTESIAN_POINT('Ctrl Pts',(11.2597624377032,4.52837111016658,333.080875681174));
#25441=CARTESIAN_POINT('Ctrl Pts',(11.2520137467954,4.47486766428751,332.954628800638));
#25442=CARTESIAN_POINT('Ctrl Pts',(11.2442650558876,4.41605318612715,332.830556028556));
#25443=CARTESIAN_POINT('Ctrl Pts',(11.2365163649798,4.35213665968466,332.709129083093));
#25444=CARTESIAN_POINT('Ctrl Pts',(11.2287692862524,4.2882334316136,332.587727401529));
#25445=CARTESIAN_POINT('Ctrl Pts',(11.221022207525,4.21923044865788,332.468970797291));
#25446=CARTESIAN_POINT('Ctrl Pts',(11.2132751287976,4.14538334322485,332.353307724685));
#25447=CARTESIAN_POINT('Ctrl Pts',(11.2055279851431,4.07153561889084,332.237643682724));
#25448=CARTESIAN_POINT('Ctrl Pts',(11.1977808414887,3.99284390144801,332.125073553557));
#25449=CARTESIAN_POINT('Ctrl Pts',(11.1900336978343,3.90960775555046,332.016017717841));
#25450=CARTESIAN_POINT('Ctrl Pts',(11.1822848124588,3.8263528964146,331.906937364076));
#25451=CARTESIAN_POINT('Ctrl Pts',(11.1745359270833,3.73855181289198,331.8013731866));
#25452=CARTESIAN_POINT('Ctrl Pts',(11.1667870417078,3.64654477865058,331.69971300645));
#25453=CARTESIAN_POINT('Ctrl Pts',(11.1590299315896,3.55444008724329,331.59794492319));
#25454=CARTESIAN_POINT('Ctrl Pts',(11.1512728214714,3.45812079008668,331.500089405032));
#25455=CARTESIAN_POINT('Ctrl Pts',(11.1435157113532,3.35796489100063,331.406498246375));
#25456=CARTESIAN_POINT('Ctrl Pts',(11.1357544560852,3.2577554718275,331.312857075617));
#25457=CARTESIAN_POINT('Ctrl Pts',(11.1279932008171,3.15370566196412,331.223485059502));
#25458=CARTESIAN_POINT('Ctrl Pts',(11.1202319455491,3.04622629221872,331.138693428502));
#25459=CARTESIAN_POINT('Ctrl Pts',(11.1124582748088,2.9385749906024,331.053766158599));
#25460=CARTESIAN_POINT('Ctrl Pts',(11.1046846040684,2.82748348300727,330.973434144725));
#25461=CARTESIAN_POINT('Ctrl Pts',(11.0969109333281,2.71339202905719,330.897965534134));
#25462=CARTESIAN_POINT('Ctrl Pts',(11.0894991329693,2.60461162047467,330.8260100457));
#25463=CARTESIAN_POINT('Ctrl Pts',(11.0820873326105,2.49310452439647,330.758475511451));
#25464=CARTESIAN_POINT('Ctrl Pts',(11.0746755322517,2.37927117827199,330.695554423303));
#25465=CARTESIAN_POINT('Ctrl Pts',(11.0669004540225,2.25985846767934,330.629549355851));
#25466=CARTESIAN_POINT('Ctrl Pts',(11.0591253757932,2.13750833988029,330.568412823143));
#25467=CARTESIAN_POINT('Ctrl Pts',(11.051350297564,2.01265554563445,330.512417051783));
#25468=CARTESIAN_POINT('Ctrl Pts',(11.0435847870634,1.88795639069944,330.456490186784));
#25469=CARTESIAN_POINT('Ctrl Pts',(11.0358192765629,1.76076105025641,330.405691654565));
#25470=CARTESIAN_POINT('Ctrl Pts',(11.0280537660624,1.63153050868936,330.360248793123));
#25471=CARTESIAN_POINT('Ctrl Pts',(11.0202959550873,1.50242809956824,330.314850988406));
#25472=CARTESIAN_POINT('Ctrl Pts',(11.0125381441123,1.37129487143893,330.274798415771));
#25473=CARTESIAN_POINT('Ctrl Pts',(11.0047803331373,1.2386131881756,330.240270970677));
#25474=CARTESIAN_POINT('Ctrl Pts',(10.9970283601597,1.10603135206214,330.205769508575));
#25475=CARTESIAN_POINT('Ctrl Pts',(10.989276387182,0.971903756963217,330.176784996093));
#25476=CARTESIAN_POINT('Ctrl Pts',(10.9815244142043,0.83672904532098,330.153447868101));
#25477=CARTESIAN_POINT('Ctrl Pts',(10.9737757241874,0.701611580171872,330.130120623383));
#25478=CARTESIAN_POINT('Ctrl Pts',(10.9660270341704,0.565448264852558,330.112436072656));
#25479=CARTESIAN_POINT('Ctrl Pts',(10.9582783441535,0.428748870367813,330.10047375059));
#25480=CARTESIAN_POINT('Ctrl Pts',(10.9505312663134,0.292077917284233,330.088513917381));
#25481=CARTESIAN_POINT('Ctrl Pts',(10.9427841884733,0.154871496029147,330.082273978787));
#25482=CARTESIAN_POINT('Ctrl Pts',(10.9350371106332,0.0176450586626147,
330.081781652427));
#25483=CARTESIAN_POINT('Ctrl Pts',(10.9272899678617,-0.119582528853916,
330.08128932194));
#25484=CARTESIAN_POINT('Ctrl Pts',(10.9195428250902,-0.256829741944676,
330.086544701175));
#25485=CARTESIAN_POINT('Ctrl Pts',(10.9117956823187,-0.393580962017785,
330.097523371923));
#25486=CARTESIAN_POINT('Ctrl Pts',(10.9040467978211,-0.530362926739534,
330.108504510916));
#25487=CARTESIAN_POINT('Ctrl Pts',(10.8962979133234,-0.666648287006521,
330.12521147058));
#25488=CARTESIAN_POINT('Ctrl Pts',(10.8885490288258,-0.801926774322948,
330.147567979752));
#25489=CARTESIAN_POINT('Ctrl Pts',(10.8807919195723,-0.937348847792901,
330.169948218383));
#25490=CARTESIAN_POINT('Ctrl Pts',(10.8730348103189,-1.07176152721795,330.197989921254));
#25491=CARTESIAN_POINT('Ctrl Pts',(10.8652777010654,-1.20466442172109,330.231565593034));
#25492=CARTESIAN_POINT('Ctrl Pts',(10.8575164466564,-1.33763833535739,330.265159206598));
#25493=CARTESIAN_POINT('Ctrl Pts',(10.8497551922474,-1.46910048204842,330.304292570055));
#25494=CARTESIAN_POINT('Ctrl Pts',(10.8419939378384,-1.59856681742754,330.348788631688));
#25495=CARTESIAN_POINT('Ctrl Pts',(10.8342202679386,-1.72824025696867,330.393355872593));
#25496=CARTESIAN_POINT('Ctrl Pts',(10.8264465980388,-1.85591114113442,330.443302811732));
#25497=CARTESIAN_POINT('Ctrl Pts',(10.8186729281391,-1.98111572953476,330.498404335273));
#25498=CARTESIAN_POINT('Ctrl Pts',(10.8112611180853,-2.10049211662678,330.550940914703));
#25499=CARTESIAN_POINT('Ctrl Pts',(10.8038493080316,-2.21762639037123,330.608162868111));
#25500=CARTESIAN_POINT('Ctrl Pts',(10.7964374979778,-2.33213997903305,330.669837626521));
#25501=CARTESIAN_POINT('Ctrl Pts',(10.7886624193224,-2.45226612264708,330.734535196239));
#25502=CARTESIAN_POINT('Ctrl Pts',(10.780887340667,-2.56988781629231,330.804337546661));
#25503=CARTESIAN_POINT('Ctrl Pts',(10.7731122620116,-2.68454087019301,330.87902640402));
#25504=CARTESIAN_POINT('Ctrl Pts',(10.7653467510906,-2.79905283613695,330.953623351936));
#25505=CARTESIAN_POINT('Ctrl Pts',(10.7575812401695,-2.91060310658166,331.03309463101));
#25506=CARTESIAN_POINT('Ctrl Pts',(10.7498157292485,-3.01875104302033,331.117175615256));
#25507=CARTESIAN_POINT('Ctrl Pts',(10.742057917859,-3.12679175039732,331.201173232909));
#25508=CARTESIAN_POINT('Ctrl Pts',(10.7343001064695,-3.23143653048037,331.289771221736));
#25509=CARTESIAN_POINT('Ctrl Pts',(10.72654229508,-3.33227307053447,331.382661303404));
#25510=CARTESIAN_POINT('Ctrl Pts',(10.7187903216942,-3.43303372783418,331.475481482284));
#25511=CARTESIAN_POINT('Ctrl Pts',(10.7110383483085,-3.52999156305906,331.572587061208));
#25512=CARTESIAN_POINT('Ctrl Pts',(10.7032863749227,-3.62276704667213,331.67362930688));
#25513=CARTESIAN_POINT('Ctrl Pts',(10.6955376845087,-3.71550323973618,331.774628761018));
#25514=CARTESIAN_POINT('Ctrl Pts',(10.6877889940946,-3.80406034023309,331.879561278677));
#25515=CARTESIAN_POINT('Ctrl Pts',(10.6800403036806,-3.88809559938438,331.988041223299));
#25516=CARTESIAN_POINT('Ctrl Pts',(10.6722932254501,-3.97211337425625,332.096498597708));
#25517=CARTESIAN_POINT('Ctrl Pts',(10.6645461472197,-4.05161093989545,332.20850162219));
#25518=CARTESIAN_POINT('Ctrl Pts',(10.6567990689892,-4.12628604724091,332.323631841685));
#25519=CARTESIAN_POINT('Ctrl Pts',(10.6490519258345,-4.2009617804004,332.438763026027));
#25520=CARTESIAN_POINT('Ctrl Pts',(10.6413047826799,-4.27081476195385,332.557021129722));
#25521=CARTESIAN_POINT('Ctrl Pts',(10.6335576395251,-4.33558649484562,332.677959343979));
#25522=CARTESIAN_POINT('Ctrl Pts',(10.6258087546516,-4.40037278976881,332.798924747661));
#25523=CARTESIAN_POINT('Ctrl Pts',(10.6180598697781,-4.46007537833466,332.922571116402));
#25524=CARTESIAN_POINT('Ctrl Pts',(10.6103109849047,-4.5144822629871,333.04842807981));
#25525=CARTESIAN_POINT('Ctrl Pts',(10.6025538752892,-4.56894689563774,333.174418629027));
#25526=CARTESIAN_POINT('Ctrl Pts',(10.5947967656736,-4.6181044407316,333.302624100607));
#25527=CARTESIAN_POINT('Ctrl Pts',(10.5870396560581,-4.66179132155541,333.432554710119));
#25528=CARTESIAN_POINT('Ctrl Pts',(10.579278401294,-4.70550154723638,333.562554750349));
#25529=CARTESIAN_POINT('Ctrl Pts',(10.5715171465298,-4.74373517471746,333.694281390203));
#25530=CARTESIAN_POINT('Ctrl Pts',(10.5637558917657,-4.77637914633891,333.827231773572));
#25531=CARTESIAN_POINT('Ctrl Pts',(10.555982221526,-4.80907533766458,333.960394834178));
#25532=CARTESIAN_POINT('Ctrl Pts',(10.5482085512865,-4.83616392784002,334.094785166774));
#25533=CARTESIAN_POINT('Ctrl Pts',(10.5404348810469,-4.85758326331165,334.229890980124));
#25534=CARTESIAN_POINT('Ctrl Pts',(10.5330230752659,-4.87800552841682,334.358707615968));
#25535=CARTESIAN_POINT('Ctrl Pts',(10.5256112694849,-4.89327443229074,334.488174334846));
#25536=CARTESIAN_POINT('Ctrl Pts',(10.5181994637039,-4.90338068022248,334.61784693208));
#25537=CARTESIAN_POINT('Ctrl Pts',(10.510978391966,-4.91322685583372,334.74418255861));
#25538=CARTESIAN_POINT('Ctrl Pts',(10.5037573202281,-4.91819124337155,334.870903575023));
#25539=CARTESIAN_POINT('Ctrl Pts',(10.4965362484902,-4.91824948156275,334.997741768903));
#25540=CARTESIAN_POINT('',(13.9965362485423,-4.91824999987318,334.999964680808));
#25541=CARTESIAN_POINT('Ctrl Pts',(13.9965362484902,-4.91824999987319,334.999964681732));
#25542=CARTESIAN_POINT('Ctrl Pts',(13.9884256421174,-4.91825103404251,335.143978065363));
#25543=CARTESIAN_POINT('Ctrl Pts',(13.9803150357447,-4.91192238318742,335.287870977352));
#25544=CARTESIAN_POINT('Ctrl Pts',(13.972204429372,-4.89932153473325,335.431081850463));
#25545=CARTESIAN_POINT('Ctrl Pts',(13.964083322496,-4.88670437242486,335.574478133416));
#25546=CARTESIAN_POINT('Ctrl Pts',(13.95596221562,-4.86779883837988,335.717190283224));
#25547=CARTESIAN_POINT('Ctrl Pts',(13.9478411087441,-4.84271384339999,335.858665064762));
#25548=CARTESIAN_POINT('Ctrl Pts',(13.9397010098725,-4.81757018472774,336.000470698789));
#25549=CARTESIAN_POINT('Ctrl Pts',(13.9315609110009,-4.78621823022439,336.141032849077));
#25550=CARTESIAN_POINT('Ctrl Pts',(13.9234208121293,-4.74881773313696,336.279809829601));
#25551=CARTESIAN_POINT('Ctrl Pts',(13.9152707060907,-4.7113712571216,336.418757417932));
#25552=CARTESIAN_POINT('Ctrl Pts',(13.9071206000521,-4.66786149995246,336.55591513884));
#25553=CARTESIAN_POINT('Ctrl Pts',(13.8989704940135,-4.61849709912264,336.690759476654));
#25554=CARTESIAN_POINT('Ctrl Pts',(13.8908017834144,-4.56902001227631,336.825911628825));
#25555=CARTESIAN_POINT('Ctrl Pts',(13.8826330728153,-4.51366168677281,336.958739529566));
#25556=CARTESIAN_POINT('Ctrl Pts',(13.8744643622162,-4.45267838032965,337.088740841714));
#25557=CARTESIAN_POINT('Ctrl Pts',(13.8686615331412,-4.40935750374523,337.181090225961));
#25558=CARTESIAN_POINT('Ctrl Pts',(13.8628587040662,-4.36319906953297,337.272013742014));
#25559=CARTESIAN_POINT('Ctrl Pts',(13.8570558749911,-4.31430829889828,337.361340078125));
#25560=CARTESIAN_POINT('Ctrl Pts',(13.8492807962115,-4.24880066660915,337.481026405496));
#25561=CARTESIAN_POINT('Ctrl Pts',(13.8415057174318,-4.17820528925671,337.598173853379));
#25562=CARTESIAN_POINT('Ctrl Pts',(13.8337306386522,-4.10274357159917,337.71231971718));
#25563=CARTESIAN_POINT('Ctrl Pts',(13.825965127602,-4.02737471438931,337.826325117228));
#25564=CARTESIAN_POINT('Ctrl Pts',(13.8181996165518,-3.94715164545592,337.937335959534));
#25565=CARTESIAN_POINT('Ctrl Pts',(13.8104341055015,-3.86234196160846,338.044913403383));
#25566=CARTESIAN_POINT('Ctrl Pts',(13.8026762939781,-3.77761636680938,338.152384183882));
#25567=CARTESIAN_POINT('Ctrl Pts',(13.7949184824547,-3.6883134475944,338.256428035543));
#25568=CARTESIAN_POINT('Ctrl Pts',(13.7871606709313,-3.59474426076282,338.356634737682));
#25569=CARTESIAN_POINT('Ctrl Pts',(13.7794086974071,-3.50124548771195,338.456766031099));
#25570=CARTESIAN_POINT('Ctrl Pts',(13.7716567238829,-3.40348710308307,338.553065638034));
#25571=CARTESIAN_POINT('Ctrl Pts',(13.7639047503587,-3.30182039623613,338.645156393558));
#25572=CARTESIAN_POINT('Ctrl Pts',(13.7561560597999,-3.20019674529963,338.737208148593));
#25573=CARTESIAN_POINT('Ctrl Pts',(13.7484073692411,-3.09466835326824,338.825054335522));
#25574=CARTESIAN_POINT('Ctrl Pts',(13.7406586786823,-2.98562316344224,338.908354818644));
#25575=CARTESIAN_POINT('Ctrl Pts',(13.7329116003032,-2.87660066137888,338.991637970405));
#25576=CARTESIAN_POINT('Ctrl Pts',(13.7251645219242,-2.76406312734088,339.070377062435));
#25577=CARTESIAN_POINT('Ctrl Pts',(13.7174174435452,-2.6484310487751,339.14427267954));
#25578=CARTESIAN_POINT('Ctrl Pts',(13.7096703002382,-2.53279800110129,339.218168915962));
#25579=CARTESIAN_POINT('Ctrl Pts',(13.7019231569312,-2.41407068653288,339.287221386012));
#25580=CARTESIAN_POINT('Ctrl Pts',(13.6941760136242,-2.29269765002026,339.351174617054));
#25581=CARTESIAN_POINT('Ctrl Pts',(13.6864271285949,-2.17129732627237,339.41514222614));
#25582=CARTESIAN_POINT('Ctrl Pts',(13.6786782435656,-2.04725044270476,339.474008132801));
#25583=CARTESIAN_POINT('Ctrl Pts',(13.6709293585364,-1.92102879119393,339.527563522018));
#25584=CARTESIAN_POINT('Ctrl Pts',(13.6631722487605,-1.79467316671826,339.581175755477));
#25585=CARTESIAN_POINT('Ctrl Pts',(13.6554151389846,-1.6661385236044,339.629466058866));
#25586=CARTESIAN_POINT('Ctrl Pts',(13.6476580292087,-1.53591574020686,339.672274168056));
#25587=CARTESIAN_POINT('Ctrl Pts',(13.6398967742814,-1.40562336991769,339.715105152531));
#25588=CARTESIAN_POINT('Ctrl Pts',(13.6321355193541,-1.27364143777154,339.752447999136));
#25589=CARTESIAN_POINT('Ctrl Pts',(13.6243742644267,-1.14047355220852,339.784193049952));
#25590=CARTESIAN_POINT('Ctrl Pts',(13.6166005940209,-1.0070926414283,339.815988882505));
#25591=CARTESIAN_POINT('Ctrl Pts',(13.6088269236151,-0.872522370068482,
339.842168950547));
#25592=CARTESIAN_POINT('Ctrl Pts',(13.6010532532093,-0.737274934218635,
339.862675059458));
#25593=CARTESIAN_POINT('Ctrl Pts',(13.5936414490453,-0.608323299292495,
339.882226604028));
#25594=CARTESIAN_POINT('Ctrl Pts',(13.5862296448812,-0.478756411163081,
339.896620515469));
#25595=CARTESIAN_POINT('Ctrl Pts',(13.5788178407172,-0.349018526858915,
339.90585050021));
#25596=CARTESIAN_POINT('Ctrl Pts',(13.5710427619398,-0.212921802153868,
339.915532874013));
#25597=CARTESIAN_POINT('Ctrl Pts',(13.5632676831624,-0.0762068045868471,
339.919562921081));
#25598=CARTESIAN_POINT('Ctrl Pts',(13.555492604385,0.0606175528599034,339.917876429394));
#25599=CARTESIAN_POINT('Ctrl Pts',(13.547727093337,0.197273539224128,339.916192013041));
#25600=CARTESIAN_POINT('Ctrl Pts',(13.5399615822891,0.334038230595531,339.908805059471));
#25601=CARTESIAN_POINT('Ctrl Pts',(13.5321960712411,0.470397784465939,339.895703114658));
#25602=CARTESIAN_POINT('Ctrl Pts',(13.5244382597199,0.606622137441573,339.882614160461));
#25603=CARTESIAN_POINT('Ctrl Pts',(13.5166804481988,0.742441765735969,339.863821528681));
#25604=CARTESIAN_POINT('Ctrl Pts',(13.5089226366776,0.877343375341519,339.839364799666));
#25605=CARTESIAN_POINT('Ctrl Pts',(13.5011706631556,1.01214346720822,339.814926475115));
#25606=CARTESIAN_POINT('Ctrl Pts',(13.4934186896336,1.14602653240934,339.784832606898));
#25607=CARTESIAN_POINT('Ctrl Pts',(13.4856667161116,1.27848530207947,339.749174496148));
#25608=CARTESIAN_POINT('Ctrl Pts',(13.477918025555,1.41088797538217,339.713531486629));
#25609=CARTESIAN_POINT('Ctrl Pts',(13.4701693349984,1.54186717620465,339.672329022805));
#25610=CARTESIAN_POINT('Ctrl Pts',(13.4624206444417,1.67092693879983,339.625709267528));
#25611=CARTESIAN_POINT('Ctrl Pts',(13.4546735660649,1.79995984943364,339.57909921188));
#25612=CARTESIAN_POINT('Ctrl Pts',(13.4469264876881,1.92707374879178,339.527074239399));
#25613=CARTESIAN_POINT('Ctrl Pts',(13.4391794093112,2.0517893023655,339.469825916207));
#25614=CARTESIAN_POINT('Ctrl Pts',(13.4314322660064,2.17650590117568,339.41257711322));
#25615=CARTESIAN_POINT('Ctrl Pts',(13.4236851227016,2.29882375887348,339.35010503527));
#25616=CARTESIAN_POINT('Ctrl Pts',(13.4159379793968,2.41828530965967,339.282648622475));
#25617=CARTESIAN_POINT('Ctrl Pts',(13.4081890943696,2.53777371793905,339.215177044045));
#25618=CARTESIAN_POINT('Ctrl Pts',(13.4004402093425,2.65440420118941,339.142719093086));
#25619=CARTESIAN_POINT('Ctrl Pts',(13.3926913243154,2.76774584874975,339.065558507663));
#25620=CARTESIAN_POINT('Ctrl Pts',(13.3849342145416,2.88120779830602,338.988316023196));
#25621=CARTESIAN_POINT('Ctrl Pts',(13.3771771047678,2.99137361534582,338.906361153738));
#25622=CARTESIAN_POINT('Ctrl Pts',(13.369419994994,3.09784288790242,338.820019961253));
#25623=CARTESIAN_POINT('Ctrl Pts',(13.3616587400688,3.20436905423441,338.733632630796));
#25624=CARTESIAN_POINT('Ctrl Pts',(13.3538974851436,3.30719444721646,338.642854565418));
#25625=CARTESIAN_POINT('Ctrl Pts',(13.3461362302183,3.40595432174344,338.548049918011));
#25626=CARTESIAN_POINT('Ctrl Pts',(13.3383625598146,3.50487217988418,338.453093614064));
#25627=CARTESIAN_POINT('Ctrl Pts',(13.3305888894108,3.59971125309843,338.354098139025));
#25628=CARTESIAN_POINT('Ctrl Pts',(13.3228152190071,3.69014542559512,338.251462717064));
#25629=CARTESIAN_POINT('Ctrl Pts',(13.3154034148191,3.7763698657418,338.153604998533));
#25630=CARTESIAN_POINT('Ctrl Pts',(13.3079916106311,3.85859009094201,338.052438809204));
#25631=CARTESIAN_POINT('Ctrl Pts',(13.3005798064431,3.93656039582682,337.948334328482));
#25632=CARTESIAN_POINT('Ctrl Pts',(13.2928047276668,4.01835225747256,337.83912737724));
#25633=CARTESIAN_POINT('Ctrl Pts',(13.2850296488905,4.0957255399037,337.726341708832));
#25634=CARTESIAN_POINT('Ctrl Pts',(13.2772545701143,4.16835084384594,337.610370530233));
#25635=CARTESIAN_POINT('Ctrl Pts',(13.2694890590674,4.24088677772781,337.494542061552));
#25636=CARTESIAN_POINT('Ctrl Pts',(13.2617235480207,4.30868615292419,337.375536210413));
#25637=CARTESIAN_POINT('Ctrl Pts',(13.2539580369738,4.37146042691334,337.253778338353));
#25638=CARTESIAN_POINT('Ctrl Pts',(13.2462002254538,4.434172460027,337.132141189579));
#25639=CARTESIAN_POINT('Ctrl Pts',(13.2384424139338,4.49186912923255,337.007757795206));
#25640=CARTESIAN_POINT('Ctrl Pts',(13.2306846024138,4.54430594564836,336.881081214314));
#25641=CARTESIAN_POINT('Ctrl Pts',(13.222932628893,4.59670330169702,336.754499961566));
#25642=CARTESIAN_POINT('Ctrl Pts',(13.2151806553722,4.64384853467592,336.625629316913));
#25643=CARTESIAN_POINT('Ctrl Pts',(13.2074286818514,4.68554390936441,336.494945261847));
#25644=CARTESIAN_POINT('Ctrl Pts',(13.199679991296,4.72722162603674,336.364316551556));
#25645=CARTESIAN_POINT('Ctrl Pts',(13.1919313007406,4.76345395634192,336.231876329916));
#25646=CARTESIAN_POINT('Ctrl Pts',(13.1841826101852,4.79409205253145,336.098118597582));
#25647=CARTESIAN_POINT('Ctrl Pts',(13.1764355318096,4.82472377420917,335.96438869466));
#25648=CARTESIAN_POINT('Ctrl Pts',(13.1686884534339,4.84976348968724,335.829342207055));
#25649=CARTESIAN_POINT('Ctrl Pts',(13.1609413750583,4.86911289559848,335.6934858848));
#25650=CARTESIAN_POINT('Ctrl Pts',(13.1531942317548,4.88846246367635,335.557628423938));
#25651=CARTESIAN_POINT('Ctrl Pts',(13.1454470884512,4.90212157195129,335.420961501859));
#25652=CARTESIAN_POINT('Ctrl Pts',(13.1376999451476,4.91004353515523,335.283999199612));
#25653=CARTESIAN_POINT('Ctrl Pts',(13.1299510601217,4.9179672793847,335.147006105331));
#25654=CARTESIAN_POINT('Ctrl Pts',(13.1222021750959,4.92015128935531,335.009717888884));
#25655=CARTESIAN_POINT('Ctrl Pts',(13.11445329007,4.91660097597461,334.872650459186));
#25656=CARTESIAN_POINT('Ctrl Pts',(13.1066961802975,4.91304689425462,334.735437544702));
#25657=CARTESIAN_POINT('Ctrl Pts',(13.098939070525,4.9037463410254,334.598446276455));
#25658=CARTESIAN_POINT('Ctrl Pts',(13.0911819607525,4.88875682285954,334.462189820249));
#25659=CARTESIAN_POINT('Ctrl Pts',(13.0834207058286,4.87375929477445,334.325860552949));
#25660=CARTESIAN_POINT('Ctrl Pts',(13.0756594509046,4.85306680321454,334.190267266305));
#25661=CARTESIAN_POINT('Ctrl Pts',(13.0678981959807,4.82678818760873,334.055913746281));
#25662=CARTESIAN_POINT('Ctrl Pts',(13.0601245255782,4.800467534782,333.921345304411));
#25663=CARTESIAN_POINT('Ctrl Pts',(13.0523508551757,4.76854299224878,333.788020972555));
#25664=CARTESIAN_POINT('Ctrl Pts',(13.0445771847733,4.73117379616419,333.656431031547));
#25665=CARTESIAN_POINT('Ctrl Pts',(13.0371653805719,4.69554414502124,333.530966633506));
#25666=CARTESIAN_POINT('Ctrl Pts',(13.0297535763706,4.65496541971395,333.407079061856));
#25667=CARTESIAN_POINT('Ctrl Pts',(13.0223417721693,4.60961594672888,333.285175260803));
#25668=CARTESIAN_POINT('Ctrl Pts',(13.0145666933827,4.56204376108948,333.157296591612));
#25669=CARTESIAN_POINT('Ctrl Pts',(13.0067916145961,4.5090710090725,333.031196950752));
#25670=CARTESIAN_POINT('Ctrl Pts',(12.9990165358095,4.45085008996464,332.907366123957));
#25671=CARTESIAN_POINT('Ctrl Pts',(12.9912510247524,4.39270081540411,332.783687678878));
#25672=CARTESIAN_POINT('Ctrl Pts',(12.9834855136953,4.32931638844699,332.66227284309));
#25673=CARTESIAN_POINT('Ctrl Pts',(12.9757200026381,4.26089835777225,332.543594445692));
#25674=CARTESIAN_POINT('Ctrl Pts',(12.9679621911077,4.19254816377381,332.425033718271));
#25675=CARTESIAN_POINT('Ctrl Pts',(12.9602043795773,4.11917449206052,332.309204366295));
#25676=CARTESIAN_POINT('Ctrl Pts',(12.9524465680469,4.04102602271569,332.196557161946));
#25677=CARTESIAN_POINT('Ctrl Pts',(12.9446945945157,3.96293636257264,332.083994728192));
#25678=CARTESIAN_POINT('Ctrl Pts',(12.9369426209846,3.88007927876489,331.974609995461));
#25679=CARTESIAN_POINT('Ctrl Pts',(12.9291906474535,3.79274802841089,331.868826824418));
#25680=CARTESIAN_POINT('Ctrl Pts',(12.9214419568877,3.70545376289335,331.76308845261));
#25681=CARTESIAN_POINT('Ctrl Pts',(12.9136932663219,3.6136893478073,331.660948909647));
#25682=CARTESIAN_POINT('Ctrl Pts',(12.9059445757562,3.51778964878551,331.562800696876));
#25683=CARTESIAN_POINT('Ctrl Pts',(12.8981974973703,3.42190990249744,331.46467290466));
#25684=CARTESIAN_POINT('Ctrl Pts',(12.8904504189844,3.32189685662842,331.370535070252));
#25685=CARTESIAN_POINT('Ctrl Pts',(12.8827033405985,3.21812345050283,331.280744090571));
#25686=CARTESIAN_POINT('Ctrl Pts',(12.8749561972846,3.11434917465628,331.190952358355));
#25687=CARTESIAN_POINT('Ctrl Pts',(12.8672090539707,3.00681477127838,331.105507809289));
#25688=CARTESIAN_POINT('Ctrl Pts',(12.8594619106568,2.89592727801453,331.024727900766));
#25689=CARTESIAN_POINT('Ctrl Pts',(12.8517130256206,2.78501485488877,330.943929831204));
#25690=CARTESIAN_POINT('Ctrl Pts',(12.8439641405845,2.67074815767828,330.867798719107));
#25691=CARTESIAN_POINT('Ctrl Pts',(12.8362152555484,2.55356395335009,330.796609202245));
#25692=CARTESIAN_POINT('Ctrl Pts',(12.8284581457657,2.43625536849858,330.725344124095));
#25693=CARTESIAN_POINT('Ctrl Pts',(12.820701035983,2.31602342522526,330.659031321944));
#25694=CARTESIAN_POINT('Ctrl Pts',(12.8129439262004,2.19333077571006,330.597900140748));
#25695=CARTESIAN_POINT('Ctrl Pts',(12.8051826712663,2.07057256316673,330.536736293005));
#25696=CARTESIAN_POINT('Ctrl Pts',(12.7974214163323,1.94535138094186,330.480759742922));
#25697=CARTESIAN_POINT('Ctrl Pts',(12.7896601613983,1.81814977266187,330.430151592594));
#25698=CARTESIAN_POINT('Ctrl Pts',(12.7818864909859,1.69074468326616,330.37946248572));
#25699=CARTESIAN_POINT('Ctrl Pts',(12.7741128205735,1.56135320625019,330.334159068585));
#25700=CARTESIAN_POINT('Ctrl Pts',(12.7663391501611,1.430473801047,330.294372755198));
#25701=CARTESIAN_POINT('Ctrl Pts',(12.7589273460726,1.30568686525819,330.256438504763));
#25702=CARTESIAN_POINT('Ctrl Pts',(12.751515541984,1.17954768845702,330.223519347463));
#25703=CARTESIAN_POINT('Ctrl Pts',(12.7441037378954,1.05249498138151,330.195685545609));
#25704=CARTESIAN_POINT('Ctrl Pts',(12.7363286591259,0.919215041222547,330.166487525899));
#25705=CARTESIAN_POINT('Ctrl Pts',(12.7285535803563,0.784508567590338,330.142793691957));
#25706=CARTESIAN_POINT('Ctrl Pts',(12.7207785015868,0.648869903754681,330.12474093914));
#25707=CARTESIAN_POINT('Ctrl Pts',(12.7130129905467,0.513398151930061,330.106710401383));
#25708=CARTESIAN_POINT('Ctrl Pts',(12.7052474795066,0.376996876094345,330.094307183815));
#25709=CARTESIAN_POINT('Ctrl Pts',(12.6974819684664,0.240172757877525,330.087617674806));
#25710=CARTESIAN_POINT('Ctrl Pts',(12.689724156953,0.103484301170844,330.080934798466));
#25711=CARTESIAN_POINT('Ctrl Pts',(12.6819663454396,-0.0336257756937801,
330.079954375664));
#25712=CARTESIAN_POINT('Ctrl Pts',(12.6742085339262,-0.170643833711854,
330.084711224708));
#25713=CARTESIAN_POINT('Ctrl Pts',(12.666456560412,-0.307558781296432,330.089464494071));
#25714=CARTESIAN_POINT('Ctrl Pts',(12.6587045868979,-0.444381458801369,
330.099946428041));
#25715=CARTESIAN_POINT('Ctrl Pts',(12.6509526133836,-0.580596734500016,
330.116139795778));
#25716=CARTESIAN_POINT('Ctrl Pts',(12.6432039228347,-0.716754322950137,
330.132326305613));
#25717=CARTESIAN_POINT('Ctrl Pts',(12.6354552322857,-0.852304633882892,
330.154219392355));
#25718=CARTESIAN_POINT('Ctrl Pts',(12.6277065417368,-0.986736389534527,
330.181749865349));
#25719=CARTESIAN_POINT('Ctrl Pts',(12.6199594633676,-1.12114017553767,330.209274610398));
#25720=CARTESIAN_POINT('Ctrl Pts',(12.6122123849984,-1.25442548647925,330.242434330338));
#25721=CARTESIAN_POINT('Ctrl Pts',(12.6044653066292,-1.38609038125846,330.281108549936));
#25722=CARTESIAN_POINT('Ctrl Pts',(12.5967181633319,-1.51775637951739,330.319783093663));
#25723=CARTESIAN_POINT('Ctrl Pts',(12.5889710200346,-1.6478015594959,330.363972119073));
#25724=CARTESIAN_POINT('Ctrl Pts',(12.5812238767374,-1.77573869307614,330.413505133938));
#25725=CARTESIAN_POINT('Ctrl Pts',(12.5734749917177,-1.90370458964197,330.463049284877));
#25726=CARTESIAN_POINT('Ctrl Pts',(12.5657261066981,-2.02956113229754,330.51793967491));
#25727=CARTESIAN_POINT('Ctrl Pts',(12.5579772216784,-2.15284101261706,330.577957639631));
#25728=CARTESIAN_POINT('Ctrl Pts',(12.550220111912,-2.27625174347826,330.638039308042));
#25729=CARTESIAN_POINT('Ctrl Pts',(12.5424630021455,-2.39707999679826,330.703259251603));
#25730=CARTESIAN_POINT('Ctrl Pts',(12.5347058923791,-2.51488254386838,330.773352527943));
#25731=CARTESIAN_POINT('Ctrl Pts',(12.5269446374611,-2.63274804085417,330.843483259889));
#25732=CARTESIAN_POINT('Ctrl Pts',(12.5191833825431,-2.747584282806,330.918492299979));
#25733=CARTESIAN_POINT('Ctrl Pts',(12.5114221276251,-2.85897784506546,330.998071871719));
#25734=CARTESIAN_POINT('Ctrl Pts',(12.5036484572285,-2.97054960072482,331.077778744841));
#25735=CARTESIAN_POINT('Ctrl Pts',(12.4958747868318,-3.07866736332111,331.162070519423));
#25736=CARTESIAN_POINT('Ctrl Pts',(12.4881011164351,-3.18295087900974,331.250599145955));
#25737=CARTESIAN_POINT('Ctrl Pts',(12.4806893121639,-3.28237997331853,331.335006744782));
#25738=CARTESIAN_POINT('Ctrl Pts',(12.4732775078927,-3.37832354385145,331.423265426778));
#25739=CARTESIAN_POINT('Ctrl Pts',(12.4658657036215,-3.47048509395734,331.515044293665));
#25740=CARTESIAN_POINT('Ctrl Pts',(12.4581989668869,-3.56581658354646,331.609979937467));
#25741=CARTESIAN_POINT('Ctrl Pts',(12.4505322301522,-3.65742082068215,331.709000872742));
#25742=CARTESIAN_POINT('Ctrl Pts',(12.4428654934176,-3.74491984483852,331.811778172988));
#25743=CARTESIAN_POINT('Ctrl Pts',(12.4352083652815,-3.83230920786664,331.914426664087));
#25744=CARTESIAN_POINT('Ctrl Pts',(12.4275512371456,-3.9156033317039,332.020821853806));
#25745=CARTESIAN_POINT('Ctrl Pts',(12.4198941090095,-3.99445959541091,332.130596646839));
#25746=CARTESIAN_POINT('Ctrl Pts',(12.412245785164,-4.07322518890332,332.24024521903));
#25747=CARTESIAN_POINT('Ctrl Pts',(12.4045974613184,-4.14756284618153,332.353265334361));
#25748=CARTESIAN_POINT('Ctrl Pts',(12.3969491374728,-4.21716938003608,332.469255942892));
#25749=CARTESIAN_POINT('Ctrl Pts',(12.3893057423903,-4.2867310577731,332.585171804298));
#25750=CARTESIAN_POINT('Ctrl Pts',(12.3816623473078,-4.35156746745738,332.704054009051));
#25751=CARTESIAN_POINT('Ctrl Pts',(12.3740189522253,-4.41141810878121,332.825471698962));
#25752=CARTESIAN_POINT('Ctrl Pts',(12.3663787195025,-4.47124398764593,332.946839153812));
#25753=CARTESIAN_POINT('Ctrl Pts',(12.3587384867798,-4.52608802306232,333.070739646857));
#25754=CARTESIAN_POINT('Ctrl Pts',(12.3510982540571,-4.57573542323469,333.196717326913));
#25755=CARTESIAN_POINT('Ctrl Pts',(12.3434594202139,-4.62537373327361,333.322671941231));
#25756=CARTESIAN_POINT('Ctrl Pts',(12.3358205863708,-4.66981715451252,333.45070261101));
#25757=CARTESIAN_POINT('Ctrl Pts',(12.3281817525277,-4.7088990670405,333.580333617034));
#25758=CARTESIAN_POINT('Ctrl Pts',(12.3205398922302,-4.74799646355784,333.710015981984));
#25759=CARTESIAN_POINT('Ctrl Pts',(12.3128980319327,-4.78172798859826,333.84129956474));
#25760=CARTESIAN_POINT('Ctrl Pts',(12.3052561716352,-4.8099769543655,333.973693632012));
#25761=CARTESIAN_POINT('Ctrl Pts',(12.2976126983372,-4.83823188276458,334.106115644274));
#25762=CARTESIAN_POINT('Ctrl Pts',(12.2899692250391,-4.8610018746485,334.239648211607));
#25763=CARTESIAN_POINT('Ctrl Pts',(12.282325751741,-4.87822163004422,334.373791735388));
#25764=CARTESIAN_POINT('Ctrl Pts',(12.2746752918931,-4.89545712523185,334.508057873636));
#25765=CARTESIAN_POINT('Ctrl Pts',(12.2670248320452,-4.90713221466497,334.642935682609));
#25766=CARTESIAN_POINT('Ctrl Pts',(12.2593743721972,-4.91323358555503,334.777921643841));
#25767=CARTESIAN_POINT('Ctrl Pts',(12.25509499764,-4.91664645901231,334.853427626431));
#25768=CARTESIAN_POINT('Ctrl Pts',(12.2508156230828,-4.91831633393994,334.928967437061));
#25769=CARTESIAN_POINT('Ctrl Pts',(12.2465362485256,-4.91824798382928,335.004453320022));
#25770=CARTESIAN_POINT('',(15.7465362484503,-4.91824799676571,334.995560989963));
#25771=CARTESIAN_POINT('Ctrl Pts',(15.7465362484503,-4.91824799676571,334.995560989963));
#25772=CARTESIAN_POINT('Ctrl Pts',(15.738885780287,-4.9183697858298,335.130498468261));
#25773=CARTESIAN_POINT('Ctrl Pts',(15.7312353121238,-4.91293416765952,335.265610303156));
#25774=CARTESIAN_POINT('Ctrl Pts',(15.7235848439605,-4.9019248808743,335.400394211703));
#25775=CARTESIAN_POINT('Ctrl Pts',(15.7159405224128,-4.89092443928026,335.535069830816));
#25776=CARTESIAN_POINT('Ctrl Pts',(15.7082962008649,-4.87435926978116,335.669417648052));
#25777=CARTESIAN_POINT('Ctrl Pts',(15.7006518793172,-4.85226517655128,335.802935687915));
#25778=CARTESIAN_POINT('Ctrl Pts',(15.6930111657414,-4.83018151130608,335.936390709846));
#25779=CARTESIAN_POINT('Ctrl Pts',(15.6853704521656,-4.80257417611059,336.069016336483));
#25780=CARTESIAN_POINT('Ctrl Pts',(15.6777297385898,-4.76953074589983,336.200316427621));
#25781=CARTESIAN_POINT('Ctrl Pts',(15.6700907439083,-4.73649474930951,336.331586980813));
#25782=CARTESIAN_POINT('Ctrl Pts',(15.6624517492269,-4.69802518718896,336.461532200858));
#25783=CARTESIAN_POINT('Ctrl Pts',(15.6548127545454,-4.65426048965109,336.58966737306));
#25784=CARTESIAN_POINT('Ctrl Pts',(15.6471737158579,-4.61049553999737,336.717803283413));
#25785=CARTESIAN_POINT('Ctrl Pts',(15.6395346771703,-4.56143552472917,336.844128743959));
#25786=CARTESIAN_POINT('Ctrl Pts',(15.6318956384828,-4.50726818798027,336.968175943385));
#25787=CARTESIAN_POINT('Ctrl Pts',(15.624254793065,-4.45308803996375,337.092252481561));
#25788=CARTESIAN_POINT('Ctrl Pts',(15.6166139476471,-4.39379833009925,337.214049318207));
#25789=CARTESIAN_POINT('Ctrl Pts',(15.6089731022292,-4.32963397083435,337.333120815795));
#25790=CARTESIAN_POINT('Ctrl Pts',(15.6013243259428,-4.26540301172684,337.452315904472));
#25791=CARTESIAN_POINT('Ctrl Pts',(15.5936755496564,-4.19628749307921,337.568779651522));
#25792=CARTESIAN_POINT('Ctrl Pts',(15.5860267733699,-4.12256726349281,337.682092880658));
#25793=CARTESIAN_POINT('Ctrl Pts',(15.5783736305095,-4.04880494811062,337.795470798652));
#25794=CARTESIAN_POINT('Ctrl Pts',(15.570720487649,-3.97043292165567,337.905694290615));
#25795=CARTESIAN_POINT('Ctrl Pts',(15.5630673447886,-3.8877721813424,338.012376226251));
#25796=CARTESIAN_POINT('Ctrl Pts',(15.555402869579,-3.80498904159278,338.119216130575));
#25797=CARTESIAN_POINT('Ctrl Pts',(15.5477383943693,-3.71790476821926,338.222503701535));
#25798=CARTESIAN_POINT('Ctrl Pts',(15.5400739191597,-3.62687844218333,338.321887389441));
#25799=CARTESIAN_POINT('Ctrl Pts',(15.5355439729847,-3.57307901741176,338.38062627822));
#25800=CARTESIAN_POINT('Ctrl Pts',(15.5310140268097,-3.51790323607385,338.438002198636));
#25801=CARTESIAN_POINT('Ctrl Pts',(15.5264840806347,-3.46143058174976,338.4939492541));
#25802=CARTESIAN_POINT('Ctrl Pts',(15.5187090018562,-3.36450242427632,338.589975287712));
#25803=CARTESIAN_POINT('Ctrl Pts',(15.5109339230777,-3.26342218309583,338.682116574258));
#25804=CARTESIAN_POINT('Ctrl Pts',(15.5031588442992,-3.15853405726114,338.769992794638));
#25805=CARTESIAN_POINT('Ctrl Pts',(15.4953933332502,-3.05377500294279,338.857760877734));
#25806=CARTESIAN_POINT('Ctrl Pts',(15.4876278222011,-2.94521768421036,338.941274088922));
#25807=CARTESIAN_POINT('Ctrl Pts',(15.4798623111521,-2.83324376524844,339.02018815843));
#25808=CARTESIAN_POINT('Ctrl Pts',(15.4721044996299,-2.72138086875325,339.099023984408));
#25809=CARTESIAN_POINT('Ctrl Pts',(15.4643466881077,-2.60610843092591,339.173269519769));
#25810=CARTESIAN_POINT('Ctrl Pts',(15.4565888765854,-2.48784160577255,339.24262032323));
#25811=CARTESIAN_POINT('Ctrl Pts',(15.4488369030624,-2.36966378015558,339.311918938013));
#25812=CARTESIAN_POINT('Ctrl Pts',(15.4410849295394,-2.24849638825972,339.376329955683));
#25813=CARTESIAN_POINT('Ctrl Pts',(15.4333329560164,-2.12478371522614,339.435592094187));
#25814=CARTESIAN_POINT('Ctrl Pts',(15.4255842654587,-2.0011234345832,339.494829135139));
#25815=CARTESIAN_POINT('Ctrl Pts',(15.4178355749011,-1.87492036850731,339.548921465377));
#25816=CARTESIAN_POINT('Ctrl Pts',(15.4100868843435,-1.74664336985366,339.597653749582));
#25817=CARTESIAN_POINT('Ctrl Pts',(15.4023398059656,-1.61839306030097,339.646375894629));
#25818=CARTESIAN_POINT('Ctrl Pts',(15.3945927275877,-1.48807004161827,339.689740073133));
#25819=CARTESIAN_POINT('Ctrl Pts',(15.3868456492099,-1.35616274235261,339.727579262028));
#25820=CARTESIAN_POINT('Ctrl Pts',(15.379098505904,-1.22425433757672,339.765418768051));
#25821=CARTESIAN_POINT('Ctrl Pts',(15.3713513625981,-1.09076200145517,339.797733084325));
#25822=CARTESIAN_POINT('Ctrl Pts',(15.3636042192923,-0.956188518868866,
339.824405308313));
#25823=CARTESIAN_POINT('Ctrl Pts',(15.3558553342642,-0.821584781306239,
339.851083528784));
#25824=CARTESIAN_POINT('Ctrl Pts',(15.3481064492361,-0.685899796948436,
339.872117056893));
#25825=CARTESIAN_POINT('Ctrl Pts',(15.3403575642079,-0.549645321806258,
339.887440340579));
#25826=CARTESIAN_POINT('Ctrl Pts',(15.3326004544332,-0.413246224756764,
339.902779888556));
#25827=CARTESIAN_POINT('Ctrl Pts',(15.3248433446585,-0.276276818489774,
339.912397041118));
#25828=CARTESIAN_POINT('Ctrl Pts',(15.3170862348837,-0.139253302482811,
339.916278224455));
#25829=CARTESIAN_POINT('Ctrl Pts',(15.3093249799575,-0.00215656548996285,
339.920161481771));
#25830=CARTESIAN_POINT('Ctrl Pts',(15.3015637250313,0.134993948217504,339.918302667632));
#25831=CARTESIAN_POINT('Ctrl Pts',(15.2938024701051,0.271684274281099,339.910740343126));
#25832=CARTESIAN_POINT('Ctrl Pts',(15.2860287997004,0.408593260318935,339.903165921366));
#25833=CARTESIAN_POINT('Ctrl Pts',(15.2782551292957,0.545040198430455,339.889869795199));
#25834=CARTESIAN_POINT('Ctrl Pts',(15.2704814588911,0.68051757418501,339.87094230039));
#25835=CARTESIAN_POINT('Ctrl Pts',(15.2630696547143,0.809688445497615,339.852895885019));
#25836=CARTESIAN_POINT('Ctrl Pts',(15.2556578505376,0.93797770610689,339.829730633964));
#25837=CARTESIAN_POINT('Ctrl Pts',(15.2482460463609,1.06495776327873,339.801567246736));
#25838=CARTESIAN_POINT('Ctrl Pts',(15.2404709675824,1.19816149131316,339.772023488006));
#25839=CARTESIAN_POINT('Ctrl Pts',(15.232695888804,1.33034538340358,339.736885893961));
#25840=CARTESIAN_POINT('Ctrl Pts',(15.2249208100256,1.46100335524586,339.696238096441));
#25841=CARTESIAN_POINT('Ctrl Pts',(15.2171552989766,1.59150054413552,339.655640318623));
#25842=CARTESIAN_POINT('Ctrl Pts',(15.2093897879276,1.7204751792831,339.609545943893));
#25843=CARTESIAN_POINT('Ctrl Pts',(15.2016242768786,1.84743121650202,339.558089617679));
#25844=CARTESIAN_POINT('Ctrl Pts',(15.1938664653564,1.97426137644032,339.506684310562));
#25845=CARTESIAN_POINT('Ctrl Pts',(15.1861086538342,2.09907656152283,339.449927777755));
#25846=CARTESIAN_POINT('Ctrl Pts',(15.178350842312,2.22139609692731,339.388004380474));
#25847=CARTESIAN_POINT('Ctrl Pts',(15.170598868789,2.34362358300259,339.326127582512));
#25848=CARTESIAN_POINT('Ctrl Pts',(15.162846895266,2.46335881024829,339.259091835239));
#25849=CARTESIAN_POINT('Ctrl Pts',(15.155094921743,2.58014163282769,339.187129352796));
#25850=CARTESIAN_POINT('Ctrl Pts',(15.1473462311854,2.69687499781225,339.115197346508));
#25851=CARTESIAN_POINT('Ctrl Pts',(15.1395975406278,2.81065811290241,339.03834295953));
#25852=CARTESIAN_POINT('Ctrl Pts',(15.1318488500702,2.92105617485242,338.956843929934));
#25853=CARTESIAN_POINT('Ctrl Pts',(15.1241017716924,3.03143126756373,338.875361856892));
#25854=CARTESIAN_POINT('Ctrl Pts',(15.1163546933145,3.13842239374486,338.789237295388));
#25855=CARTESIAN_POINT('Ctrl Pts',(15.1086076149367,3.24162478342162,338.69879058964));
#25856=CARTESIAN_POINT('Ctrl Pts',(15.1008604716309,3.34482803803353,338.608343125861));
#25857=CARTESIAN_POINT('Ctrl Pts',(15.0931133283251,3.44424219884817,338.513573703215));
#25858=CARTESIAN_POINT('Ctrl Pts',(15.0853661850193,3.53949687427885,338.414841861561));
#25859=CARTESIAN_POINT('Ctrl Pts',(15.0776172999912,3.63477296498288,338.316087822894));
#25860=CARTESIAN_POINT('Ctrl Pts',(15.0698684149631,3.72588743813857,338.213369873799));
#25861=CARTESIAN_POINT('Ctrl Pts',(15.062119529935,3.81250822907731,338.107082886844));
#25862=CARTESIAN_POINT('Ctrl Pts',(15.0543624201603,3.89922096021863,338.000683085782));
#25863=CARTESIAN_POINT('Ctrl Pts',(15.0466053103856,3.98143023401501,337.890706983022));
#25864=CARTESIAN_POINT('Ctrl Pts',(15.0388482006109,4.05884529080318,337.77758131615));
#25865=CARTESIAN_POINT('Ctrl Pts',(15.0310869456848,4.13630171572239,337.664395198538));
#25866=CARTESIAN_POINT('Ctrl Pts',(15.0233256907586,4.20895861191853,337.548056494595));
#25867=CARTESIAN_POINT('Ctrl Pts',(15.0155644358325,4.27657027062901,337.429018275533));
#25868=CARTESIAN_POINT('Ctrl Pts',(15.0077907654278,4.34429008595892,337.309789634114));
#25869=CARTESIAN_POINT('Ctrl Pts',(15.0000170950231,4.40694835734054,337.187853196088));
#25870=CARTESIAN_POINT('Ctrl Pts',(14.9922434246185,4.46434640486665,337.063684627033));
#25871=CARTESIAN_POINT('Ctrl Pts',(14.9848316204413,4.51907255947218,336.945296134739));
#25872=CARTESIAN_POINT('Ctrl Pts',(14.977419816264,4.56901708580637,336.824878911986));
#25873=CARTESIAN_POINT('Ctrl Pts',(14.9700080120868,4.61405008770027,336.702857848058));
#25874=CARTESIAN_POINT('Ctrl Pts',(14.9622329333085,4.66129029116216,336.574856168308));
#25875=CARTESIAN_POINT('Ctrl Pts',(14.9544578545301,4.70327462742217,336.444684945099));
#25876=CARTESIAN_POINT('Ctrl Pts',(14.9466827757517,4.739799553021,336.312815013504));
#25877=CARTESIAN_POINT('Ctrl Pts',(14.9389172647028,4.77627953237354,336.181107356256));
#25878=CARTESIAN_POINT('Ctrl Pts',(14.9311517536538,4.80731336492425,336.047705522947));
#25879=CARTESIAN_POINT('Ctrl Pts',(14.9233862426049,4.83274583891294,335.913099512085));
#25880=CARTESIAN_POINT('Ctrl Pts',(14.9156284310828,4.85815309652964,335.778626963474));
#25881=CARTESIAN_POINT('Ctrl Pts',(14.9078706195607,4.87796997578691,335.642952994933));
#25882=CARTESIAN_POINT('Ctrl Pts',(14.9001128080386,4.89209138923601,335.506581584607));
#25883=CARTESIAN_POINT('Ctrl Pts',(14.8923608345156,4.90620217587365,335.370312798092));
#25884=CARTESIAN_POINT('Ctrl Pts',(14.8846088609927,4.9146259877156,335.233348001703));
#25885=CARTESIAN_POINT('Ctrl Pts',(14.8768568874698,4.91730908727221,335.096199806289));
#25886=CARTESIAN_POINT('Ctrl Pts',(14.8691081969122,4.91999105053457,334.959109693217));
#25887=CARTESIAN_POINT('Ctrl Pts',(14.8613595063547,4.91693712935775,334.821836725585));
#25888=CARTESIAN_POINT('Ctrl Pts',(14.8536108157971,4.90814558262637,334.684896838725));
#25889=CARTESIAN_POINT('Ctrl Pts',(14.8458637374194,4.89935586504974,334.547985443353));
#25890=CARTESIAN_POINT('Ctrl Pts',(14.8381166590416,4.88483092142032,334.411407380737));
#25891=CARTESIAN_POINT('Ctrl Pts',(14.8303695806639,4.86462109176771,334.275676387221));
#25892=CARTESIAN_POINT('Ctrl Pts',(14.8226224373582,4.84441109273728,334.13994425615));
#25893=CARTESIAN_POINT('Ctrl Pts',(14.8148752940525,4.81851617021758,334.005059594951));
#25894=CARTESIAN_POINT('Ctrl Pts',(14.8071281507467,4.78703822880825,333.871528441462));
#25895=CARTESIAN_POINT('Ctrl Pts',(14.7993792657187,4.7555532104894,333.737967267335));
#25896=CARTESIAN_POINT('Ctrl Pts',(14.7916303806907,4.71848276527753,333.605760586808));
#25897=CARTESIAN_POINT('Ctrl Pts',(14.7838814956627,4.67597925069131,333.475401328348));
#25898=CARTESIAN_POINT('Ctrl Pts',(14.776124385888,4.63343062243545,333.344903705223));
#25899=CARTESIAN_POINT('Ctrl Pts',(14.7683672761133,4.58543752660682,333.216257793399));
#25900=CARTESIAN_POINT('Ctrl Pts',(14.7606101663387,4.53220146920776,333.089939031075));
#25901=CARTESIAN_POINT('Ctrl Pts',(14.7528489114126,4.47893696416181,332.963552768043));
#25902=CARTESIAN_POINT('Ctrl Pts',(14.7450876564865,4.4204240816234,332.839496485748));
#25903=CARTESIAN_POINT('Ctrl Pts',(14.7373264015604,4.35691085173058,332.718221988761));
#25904=CARTESIAN_POINT('Ctrl Pts',(14.7295527311558,4.29329602136885,332.596753492103));
#25905=CARTESIAN_POINT('Ctrl Pts',(14.7217790607513,4.22466505521,332.478076011616));
#25906=CARTESIAN_POINT('Ctrl Pts',(14.7140053903467,4.15131043348857,332.362614031411));
#25907=CARTESIAN_POINT('Ctrl Pts',(14.7065935861687,4.08137048704784,332.25252683415));
#25908=CARTESIAN_POINT('Ctrl Pts',(14.6991817819908,4.00713692445492,332.145362747655));
#25909=CARTESIAN_POINT('Ctrl Pts',(14.6917699778129,3.92889674990318,332.041460936357));
#25910=CARTESIAN_POINT('Ctrl Pts',(14.6839948990343,3.84682179133859,331.93246658779));
#25911=CARTESIAN_POINT('Ctrl Pts',(14.6762198202557,3.76007816606868,331.826717945627));
#25912=CARTESIAN_POINT('Ctrl Pts',(14.6684447414771,3.66895166030728,331.724640969782));
#25913=CARTESIAN_POINT('Ctrl Pts',(14.6606792304279,3.5779372915125,331.622689606154));
#25914=CARTESIAN_POINT('Ctrl Pts',(14.6529137193787,3.48255103139087,331.524401207683));
#25915=CARTESIAN_POINT('Ctrl Pts',(14.6451482083295,3.38312093615007,331.430171461557));
#25916=CARTESIAN_POINT('Ctrl Pts',(14.6373903968071,3.28378942613852,331.336035144498));
#25917=CARTESIAN_POINT('Ctrl Pts',(14.6296325852847,3.18042234197027,331.245949738606));
#25918=CARTESIAN_POINT('Ctrl Pts',(14.6218747737624,3.07338662077073,331.160276345651));
#25919=CARTESIAN_POINT('Ctrl Pts',(14.6141228002392,2.96643144734554,331.07466742464));
#25920=CARTESIAN_POINT('Ctrl Pts',(14.606370826716,2.85581343598871,330.993464151183));
#25921=CARTESIAN_POINT('Ctrl Pts',(14.5986188531928,2.74193457165876,330.916989117423));
#25922=CARTESIAN_POINT('Ctrl Pts',(14.5908701626351,2.62810393509546,330.840546470885));
#25923=CARTESIAN_POINT('Ctrl Pts',(14.5831214720773,2.51101551603632,330.768828298848));
#25924=CARTESIAN_POINT('Ctrl Pts',(14.5753727815195,2.39110223329226,330.702115267664));
#25925=CARTESIAN_POINT('Ctrl Pts',(14.5676257031415,2.27121389950805,330.635416116684));
#25926=CARTESIAN_POINT('Ctrl Pts',(14.5598786247635,2.1485022124451,330.573720225129));
#25927=CARTESIAN_POINT('Ctrl Pts',(14.5521315463855,2.02342642583465,330.517263273208));
#25928=CARTESIAN_POINT('Ctrl Pts',(14.5443844030795,1.89834959096864,330.460805848123));
#25929=CARTESIAN_POINT('Ctrl Pts',(14.5366372597734,1.77090897329795,330.409587611059));
#25930=CARTESIAN_POINT('Ctrl Pts',(14.5288901164674,1.64158525726161,330.363796714375));
#25931=CARTESIAN_POINT('Ctrl Pts',(14.5211412314391,1.51223246650829,330.317995522925));
#25932=CARTESIAN_POINT('Ctrl Pts',(14.5133923464109,1.38099610333606,330.277624230317));
#25933=CARTESIAN_POINT('Ctrl Pts',(14.5056434613826,1.24837313120486,330.242821467741));
#25934=CARTESIAN_POINT('Ctrl Pts',(14.4978863516077,1.11560939168097,330.207981765153));
#25935=CARTESIAN_POINT('Ctrl Pts',(14.4901292418328,0.981456481887707,330.178722498737));
#25936=CARTESIAN_POINT('Ctrl Pts',(14.4823721320579,0.846423254408913,330.155131504685));
#25937=CARTESIAN_POINT('Ctrl Pts',(14.4746108771315,0.711317869490973,330.13152790436));
#25938=CARTESIAN_POINT('Ctrl Pts',(14.4668496222053,0.575331616870021,330.113598662909));
#25939=CARTESIAN_POINT('Ctrl Pts',(14.4590883672789,0.438978651988007,330.101379703876));
#25940=CARTESIAN_POINT('Ctrl Pts',(14.4513146968741,0.302407566799698,330.08914119849));
#25941=CARTESIAN_POINT('Ctrl Pts',(14.4435410264693,0.165468987748349,330.08263124771));
#25942=CARTESIAN_POINT('Ctrl Pts',(14.4357673560644,0.0286781504160663,
330.081833611376));
#25943=CARTESIAN_POINT('Ctrl Pts',(14.4283555518893,-0.101745040491597,
330.081073105206));
#25944=CARTESIAN_POINT('Ctrl Pts',(14.4209437477141,-0.23203364726224,330.085505055417));
#25945=CARTESIAN_POINT('Ctrl Pts',(14.413531943539,-0.361747144852734,330.095071655397));
#25946=CARTESIAN_POINT('Ctrl Pts',(14.4057568647607,-0.497818287390422,
330.105107142942));
#25947=CARTESIAN_POINT('Ctrl Pts',(14.3979817859823,-0.633686529610552,
330.120825049894));
#25948=CARTESIAN_POINT('Ctrl Pts',(14.390206707204,-0.768839017416416,330.142215563881));
#25949=CARTESIAN_POINT('Ctrl Pts',(14.3824411961551,-0.903825191481438,
330.163579755479));
#25950=CARTESIAN_POINT('Ctrl Pts',(14.3746756851063,-1.03809698125641,330.19060260439));
#25951=CARTESIAN_POINT('Ctrl Pts',(14.3669101740574,-1.17114411490555,330.223222370193));
#25952=CARTESIAN_POINT('Ctrl Pts',(14.3591523625353,-1.30405933193441,330.255809793404));
#25953=CARTESIAN_POINT('Ctrl Pts',(14.3513945510132,-1.43575193207844,330.293982997491));
#25954=CARTESIAN_POINT('Ctrl Pts',(14.3436367394911,-1.56571968642209,330.337628830085));
#25955=CARTESIAN_POINT('Ctrl Pts',(14.3358847659682,-1.69558963590908,330.381241817807));
#25956=CARTESIAN_POINT('Ctrl Pts',(14.3281327924454,-1.82373695415702,330.430319112775));
#25957=CARTESIAN_POINT('Ctrl Pts',(14.3203808189225,-1.94967282942241,330.484697250382));
#25958=CARTESIAN_POINT('Ctrl Pts',(14.312632128365,-2.0755553707702,330.539052358815));
#25959=CARTESIAN_POINT('Ctrl Pts',(14.3048834378075,-2.19922797375872,330.598703690293));
#25960=CARTESIAN_POINT('Ctrl Pts',(14.29713474725,-2.32022034285369,330.66343907882));
#25961=CARTESIAN_POINT('Ctrl Pts',(14.2893876688722,-2.44118753847572,330.728160998609));
#25962=CARTESIAN_POINT('Ctrl Pts',(14.2816405904945,-2.55947526497103,330.797964687164));
#25963=CARTESIAN_POINT('Ctrl Pts',(14.2738935121168,-2.67463680527738,330.872591488312));
#25964=CARTESIAN_POINT('Ctrl Pts',(14.2661463688111,-2.78979931074804,330.947218914903));
#25965=CARTESIAN_POINT('Ctrl Pts',(14.2583992255054,-2.90183524974824,331.026669322147));
#25966=CARTESIAN_POINT('Ctrl Pts',(14.2506520821997,-3.01032627501437,331.11064031228));
#25967=CARTESIAN_POINT('Ctrl Pts',(14.2429031971717,-3.11884169136691,331.194630180875));
#25968=CARTESIAN_POINT('Ctrl Pts',(14.2351543121436,-3.22381029905678,331.283142415532));
#25969=CARTESIAN_POINT('Ctrl Pts',(14.2274054271156,-3.32484658471488,331.375834130367));
#25970=CARTESIAN_POINT('Ctrl Pts',(14.219648317341,-3.42599011133021,331.468624229146));
#25971=CARTESIAN_POINT('Ctrl Pts',(14.2118912075664,-3.52319268985944,331.565602405058));
#25972=CARTESIAN_POINT('Ctrl Pts',(14.2041340977918,-3.61610508764279,331.666388286314));
#25973=CARTESIAN_POINT('Ctrl Pts',(14.1963728428657,-3.70906713484093,331.767228024323));
#25974=CARTESIAN_POINT('Ctrl Pts',(14.1886115879396,-3.79773418066319,331.871879223957));
#25975=CARTESIAN_POINT('Ctrl Pts',(14.1808503330135,-3.8817977772239,331.979928961226));
#25976=CARTESIAN_POINT('Ctrl Pts',(14.1730766626089,-3.96599584814273,332.088151542862));
#25977=CARTESIAN_POINT('Ctrl Pts',(14.1653029922044,-4.04557552729667,332.199783207529));
#25978=CARTESIAN_POINT('Ctrl Pts',(14.1575293217998,-4.12027164784493,332.314381894151));
#25979=CARTESIAN_POINT('Ctrl Pts',(14.1501175176215,-4.19149064602285,332.423645984358));
#25980=CARTESIAN_POINT('Ctrl Pts',(14.1427057134433,-4.25827036565018,332.535606835987));
#25981=CARTESIAN_POINT('Ctrl Pts',(14.135293909265,-4.3204210241634,332.649862719655));
#25982=CARTESIAN_POINT('Ctrl Pts',(14.1271138568986,-4.38901372157135,332.775961452041));
#25983=CARTESIAN_POINT('Ctrl Pts',(14.1189338045322,-4.45216623723888,332.905220028662));
#25984=CARTESIAN_POINT('Ctrl Pts',(14.1107537521658,-4.50959184349229,333.0371539878));
#25985=CARTESIAN_POINT('Ctrl Pts',(14.102587857685,-4.56691805855238,333.168859598045));
#25986=CARTESIAN_POINT('Ctrl Pts',(14.0944219632042,-4.61853698427458,333.303231061453));
#25987=CARTESIAN_POINT('Ctrl Pts',(14.0862560687234,-4.66420741630333,333.439758916));
#25988=CARTESIAN_POINT('Ctrl Pts',(14.0781089270173,-4.70977296731469,333.575973237706));
#25989=CARTESIAN_POINT('Ctrl Pts',(14.0699617853112,-4.7494171610063,333.7143337624));
#25990=CARTESIAN_POINT('Ctrl Pts',(14.0618146436051,-4.78294686407446,333.854311404464));
#25991=CARTESIAN_POINT('Ctrl Pts',(14.0536786667445,-4.81643061802757,333.994097221127));
#25992=CARTESIAN_POINT('Ctrl Pts',(14.0455426898837,-4.84381649802361,334.13549541966));
#25993=CARTESIAN_POINT('Ctrl Pts',(14.037406713023,-4.86496063921135,334.277960498709));
#25994=CARTESIAN_POINT('Ctrl Pts',(14.0292854251914,-4.88606660589207,334.420168365413));
#25995=CARTESIAN_POINT('Ctrl Pts',(14.02116413736,-4.90095325625342,334.563438945091));
#25996=CARTESIAN_POINT('Ctrl Pts',(14.0130428495284,-4.90952752261186,334.707215835099));
#25997=CARTESIAN_POINT('Ctrl Pts',(14.0075406492106,-4.91533661743288,334.804625170454));
#25998=CARTESIAN_POINT('Ctrl Pts',(14.0020384488928,-4.91824929826728,334.902266623046));
#25999=CARTESIAN_POINT('Ctrl Pts',(13.996536248575,-4.91824999987318,334.999964680227));
#26000=CARTESIAN_POINT('',(17.4965362485264,-4.91824945026714,335.002325391798));
#26001=CARTESIAN_POINT('Ctrl Pts',(17.4965362484902,-4.91824945026684,335.002325392432));
#26002=CARTESIAN_POINT('Ctrl Pts',(17.4890742725109,-4.91818747571447,335.133402755509));
#26003=CARTESIAN_POINT('Ctrl Pts',(17.4816122965316,-4.91288593130427,335.264351668712));
#26004=CARTESIAN_POINT('Ctrl Pts',(17.4741503205523,-4.90237255421105,335.394875172957));
#26005=CARTESIAN_POINT('Ctrl Pts',(17.4663752417739,-4.89141803822839,335.530875413479));
#26006=CARTESIAN_POINT('Ctrl Pts',(17.4586001629954,-4.87478260324696,335.666634369524));
#26007=CARTESIAN_POINT('Ctrl Pts',(17.450825084217,-4.85247952611126,335.801639264988));
#26008=CARTESIAN_POINT('Ctrl Pts',(17.443059573168,-4.83020389433186,335.936478028334));
#26009=CARTESIAN_POINT('Ctrl Pts',(17.435294062119,-4.80227456054411,336.070564195434));
#26010=CARTESIAN_POINT('Ctrl Pts',(17.4275285510699,-4.76875671101047,336.203387923195));
#26011=CARTESIAN_POINT('Ctrl Pts',(17.4197707395477,-4.73527209452216,336.336079955845));
#26012=CARTESIAN_POINT('Ctrl Pts',(17.4120129280255,-4.6962100842725,336.467511663582));
#26013=CARTESIAN_POINT('Ctrl Pts',(17.4042551165033,-4.65168722296251,336.597181593379));
#26014=CARTESIAN_POINT('Ctrl Pts',(17.3965031429803,-4.60719786651756,336.726753942441));
#26015=CARTESIAN_POINT('Ctrl Pts',(17.3887511694572,-4.55725596512239,336.854566784288));
#26016=CARTESIAN_POINT('Ctrl Pts',(17.3809991959342,-4.5020282819259,336.980132422652));
#26017=CARTESIAN_POINT('Ctrl Pts',(17.3732505053766,-4.44682398768617,337.105644883894));
#26018=CARTESIAN_POINT('Ctrl Pts',(17.3655018148189,-4.38633852096908,337.228911677449));
#26019=CARTESIAN_POINT('Ctrl Pts',(17.3577531242613,-4.32078722010939,337.349463951849));
#26020=CARTESIAN_POINT('Ctrl Pts',(17.3500060458835,-4.25524955774524,337.469991144342));
#26021=CARTESIAN_POINT('Ctrl Pts',(17.3422589675056,-4.18464834430203,337.587804597887));
#26022=CARTESIAN_POINT('Ctrl Pts',(17.3345118891278,-4.10924524794454,337.702459353024));
#26023=CARTESIAN_POINT('Ctrl Pts',(17.3267647458219,-4.03384151963658,337.817115069077));
#26024=CARTESIAN_POINT('Ctrl Pts',(17.3190176025161,-3.95363604291983,337.928611707341));
#26025=CARTESIAN_POINT('Ctrl Pts',(17.3112704592103,-3.86893403488975,338.036532973009));
#26026=CARTESIAN_POINT('Ctrl Pts',(17.3035215741822,-3.78421298404988,338.144478501669));
#26027=CARTESIAN_POINT('Ctrl Pts',(17.2957726891541,-3.69499363156641,338.248846750803));
#26028=CARTESIAN_POINT('Ctrl Pts',(17.2880238041259,-3.60162145991608,338.349254532276));
#26029=CARTESIAN_POINT('Ctrl Pts',(17.2802666943512,-3.50815018207818,338.449768887606));
#26030=CARTESIAN_POINT('Ctrl Pts',(17.2725095845765,-3.41051754658914,338.546314091339));
#26031=CARTESIAN_POINT('Ctrl Pts',(17.2647524748018,-3.3091062758736,338.638543488468));
#26032=CARTESIAN_POINT('Ctrl Pts',(17.2569912198756,-3.20764081421757,338.730822170038));
#26033=CARTESIAN_POINT('Ctrl Pts',(17.2492299649494,-3.10239299370636,338.818780199107));
#26034=CARTESIAN_POINT('Ctrl Pts',(17.2414687100232,-2.99377781269178,338.902111924424));
#26035=CARTESIAN_POINT('Ctrl Pts',(17.2336950396186,-2.88498888278518,338.985576953344));
#26036=CARTESIAN_POINT('Ctrl Pts',(17.2259213692139,-2.77282214816773,339.064400665108));
#26037=CARTESIAN_POINT('Ctrl Pts',(17.2181476988092,-2.65772145121774,339.138320885364));
#26038=CARTESIAN_POINT('Ctrl Pts',(17.2107358946323,-2.54797871940428,339.208800101581));
#26039=CARTESIAN_POINT('Ctrl Pts',(17.2033240904553,-2.43556927819767,339.27482192201));
#26040=CARTESIAN_POINT('Ctrl Pts',(17.1959122862783,-2.32089612992976,339.336199282387));
#26041=CARTESIAN_POINT('Ctrl Pts',(17.1881372074999,-2.20060250906958,339.400584930031));
#26042=CARTESIAN_POINT('Ctrl Pts',(17.1803621287215,-2.07743751823178,339.460062798817));
#26043=CARTESIAN_POINT('Ctrl Pts',(17.172587049943,-1.95183954664401,339.514366560954));
#26044=CARTESIAN_POINT('Ctrl Pts',(17.164821538894,-1.82639613135625,339.568603498854));
#26045=CARTESIAN_POINT('Ctrl Pts',(17.157056027845,-1.69852604774229,339.617678845105));
#26046=CARTESIAN_POINT('Ctrl Pts',(17.149290516796,-1.56869330976127,339.661371510876));
#26047=CARTESIAN_POINT('Ctrl Pts',(17.1415327052739,-1.43898930131803,339.705020855242));
#26048=CARTESIAN_POINT('Ctrl Pts',(17.1337748937516,-1.30732687918569,339.743298016078));
#26049=CARTESIAN_POINT('Ctrl Pts',(17.1260170822294,-1.17419079385777,339.776029631621));
#26050=CARTESIAN_POINT('Ctrl Pts',(17.1182651087064,-1.04115489765623,339.808736615585));
#26051=CARTESIAN_POINT('Ctrl Pts',(17.1105131351835,-0.906647923669278,
339.835906267861));
#26052=CARTESIAN_POINT('Ctrl Pts',(17.1027611616605,-0.771170231202778,
339.857414902704));
#26053=CARTESIAN_POINT('Ctrl Pts',(17.0950124711029,-0.63574991361947,339.878914428627));
#26054=CARTESIAN_POINT('Ctrl Pts',(17.0872637805453,-0.499360080441308,
339.894757644304));
#26055=CARTESIAN_POINT('Ctrl Pts',(17.0795150899877,-0.362511530800745,
339.904871909901));
#26056=CARTESIAN_POINT('Ctrl Pts',(17.0717680116099,-0.22569145364373,339.914984071141));
#26057=CARTESIAN_POINT('Ctrl Pts',(17.0640209332321,-0.088413239427148,
339.919369624394));
#26058=CARTESIAN_POINT('Ctrl Pts',(17.0562738548543,0.0488073322865175,
339.918007818905));
#26059=CARTESIAN_POINT('Ctrl Pts',(17.0485267115485,0.186029054040741,339.916646002004));
#26060=CARTESIAN_POINT('Ctrl Pts',(17.0407795682426,0.323192741473425,339.909536734164));
#26061=CARTESIAN_POINT('Ctrl Pts',(17.0330324249368,0.459783152918351,339.896711397948));
#26062=CARTESIAN_POINT('Ctrl Pts',(17.0252835399088,0.596404272787481,339.883883178324));
#26063=CARTESIAN_POINT('Ctrl Pts',(17.0175346548807,0.732451471116397,339.865336369664));
#26064=CARTESIAN_POINT('Ctrl Pts',(17.0097857698526,0.867415556436818,339.841154130468));
#26065=CARTESIAN_POINT('Ctrl Pts',(17.0020286600779,1.00252289403202,339.816946223994));
#26066=CARTESIAN_POINT('Ctrl Pts',(16.9942715503032,1.13654443677542,339.787091007413));
#26067=CARTESIAN_POINT('Ctrl Pts',(16.9865144405285,1.26898156201064,339.751722725263));
#26068=CARTESIAN_POINT('Ctrl Pts',(16.9787531856023,1.40148945741097,339.716335543433));
#26069=CARTESIAN_POINT('Ctrl Pts',(16.9709919306761,1.53241087535465,339.675429542361));
#26070=CARTESIAN_POINT('Ctrl Pts',(16.96323067575,1.66126420776291,339.629188297586));
#26071=CARTESIAN_POINT('Ctrl Pts',(16.9554570053454,1.79032366350981,339.582873081889));
#26072=CARTESIAN_POINT('Ctrl Pts',(16.9476833349407,1.9173080605895,339.531205715116));
#26073=CARTESIAN_POINT('Ctrl Pts',(16.9399096645361,2.04175674241726,339.474417556207));
#26074=CARTESIAN_POINT('Ctrl Pts',(16.9324978603589,2.16041230816699,339.420272899757));
#26075=CARTESIAN_POINT('Ctrl Pts',(16.9250860561817,2.27676266417264,339.36147359786));
#26076=CARTESIAN_POINT('Ctrl Pts',(16.9176742520045,2.39043241641722,339.298257312568));
#26077=CARTESIAN_POINT('Ctrl Pts',(16.9098991732261,2.50967346182275,339.231942608822));
#26078=CARTESIAN_POINT('Ctrl Pts',(16.9021240944476,2.62634131433764,339.160557428056));
#26079=CARTESIAN_POINT('Ctrl Pts',(16.8943490156691,2.73997477567468,339.084326295874));
#26080=CARTESIAN_POINT('Ctrl Pts',(16.8865835046201,2.85346840380328,339.008188970953));
#26081=CARTESIAN_POINT('Ctrl Pts',(16.8788179935711,2.96393474887053,338.927217775453));
#26082=CARTESIAN_POINT('Ctrl Pts',(16.8710524825221,3.0709367879821,338.841683264758));
#26083=CARTESIAN_POINT('Ctrl Pts',(16.8632946709999,3.17783273426029,338.756233561779));
#26084=CARTESIAN_POINT('Ctrl Pts',(16.8555368594777,3.28127090681902,338.666229790184));
#26085=CARTESIAN_POINT('Ctrl Pts',(16.8477790479555,3.38084319574525,338.571985771008));
#26086=CARTESIAN_POINT('Ctrl Pts',(16.8400270744324,3.48034055336644,338.477812673445));
#26087=CARTESIAN_POINT('Ctrl Pts',(16.8322751009094,3.57597753523768,338.379405947279));
#26088=CARTESIAN_POINT('Ctrl Pts',(16.8245231273864,3.6673793582458,338.277119421872));
#26089=CARTESIAN_POINT('Ctrl Pts',(16.8167744368288,3.75874247252761,338.17487621487));
#26090=CARTESIAN_POINT('Ctrl Pts',(16.8090257462711,3.84587373537039,338.068756767487));
#26091=CARTESIAN_POINT('Ctrl Pts',(16.8012770557135,3.92843563966845,337.959151312029));
#26092=CARTESIAN_POINT('Ctrl Pts',(16.7935299773357,4.01098036627276,337.849568660902));
#26093=CARTESIAN_POINT('Ctrl Pts',(16.7857828989578,4.08895739029967,337.736501756372));
#26094=CARTESIAN_POINT('Ctrl Pts',(16.77803582058,4.16207014408058,337.620373099055));
#26095=CARTESIAN_POINT('Ctrl Pts',(16.7702886772742,4.2351835106167,337.504243468468));
#26096=CARTESIAN_POINT('Ctrl Pts',(16.7625415339684,4.30343231734124,337.385052364689));
#26097=CARTESIAN_POINT('Ctrl Pts',(16.7547943906626,4.36656412768936,337.263250048332));
#26098=CARTESIAN_POINT('Ctrl Pts',(16.7470455056345,4.42971013140886,337.141420348228));
#26099=CARTESIAN_POINT('Ctrl Pts',(16.7392966206063,4.48773666973072,337.016978614332));
#26100=CARTESIAN_POINT('Ctrl Pts',(16.7315477355782,4.5404381196899,336.890398038448));
#26101=CARTESIAN_POINT('Ctrl Pts',(16.7237906258035,4.59319550751257,336.763683108632));
#26102=CARTESIAN_POINT('Ctrl Pts',(16.7160335160287,4.64061636588967,336.634825163331));
#26103=CARTESIAN_POINT('Ctrl Pts',(16.708276406254,4.68254375058519,336.504316152395));
#26104=CARTESIAN_POINT('Ctrl Pts',(16.7005151513278,4.72449353993449,336.373737401616));
#26105=CARTESIAN_POINT('Ctrl Pts',(16.6927538964016,4.76094390246089,336.241506203815));
#26106=CARTESIAN_POINT('Ctrl Pts',(16.6849926414754,4.791788584984,336.108126896757));
#26107=CARTESIAN_POINT('Ctrl Pts',(16.6772189710708,4.8226826089469,335.974534226276));
#26108=CARTESIAN_POINT('Ctrl Pts',(16.6694453006661,4.84795296157558,335.839790160845));
#26109=CARTESIAN_POINT('Ctrl Pts',(16.6616716302614,4.86754490982744,335.70440727801));
#26110=CARTESIAN_POINT('Ctrl Pts',(16.6542598260844,4.88622484817441,335.575326500943));
#26111=CARTESIAN_POINT('Ctrl Pts',(16.6468480219074,4.89974311459746,335.445665328196));
#26112=CARTESIAN_POINT('Ctrl Pts',(16.6394362177304,4.90809641694306,335.315868049177));
#26113=CARTESIAN_POINT('Ctrl Pts',(16.631661138952,4.91685913951992,335.179709018866));
#26114=CARTESIAN_POINT('Ctrl Pts',(16.6238860601735,4.91996548747335,335.042969915293));
#26115=CARTESIAN_POINT('Ctrl Pts',(16.6161109813951,4.9173546883175,334.906160073626));
#26116=CARTESIAN_POINT('Ctrl Pts',(16.6083454703461,4.91474710191623,334.769518585179));
#26117=CARTESIAN_POINT('Ctrl Pts',(16.600579959297,4.90643637404882,334.632806918904));
#26118=CARTESIAN_POINT('Ctrl Pts',(16.592814448248,4.89241352234543,334.496538989721));
#26119=CARTESIAN_POINT('Ctrl Pts',(16.5850566367258,4.87840457434035,334.360406170586));
#26120=CARTESIAN_POINT('Ctrl Pts',(16.5772988252036,4.85869481311291,334.224716599299));
#26121=CARTESIAN_POINT('Ctrl Pts',(16.5695410136814,4.83332728577409,334.089983290762));
#26122=CARTESIAN_POINT('Ctrl Pts',(16.5617890401584,4.80797884830404,333.955351373313));
#26123=CARTESIAN_POINT('Ctrl Pts',(16.5540370666353,4.77698119139533,333.821674668827));
#26124=CARTESIAN_POINT('Ctrl Pts',(16.5462850931123,4.74042904105868,333.68945981779));
#26125=CARTESIAN_POINT('Ctrl Pts',(16.5385364025547,4.70389237057945,333.557300959821));
#26126=CARTESIAN_POINT('Ctrl Pts',(16.5307877119971,4.66180598923088,333.426603099921));
#26127=CARTESIAN_POINT('Ctrl Pts',(16.5230390214394,4.61431540722336,333.297861232108));
#26128=CARTESIAN_POINT('Ctrl Pts',(16.5152919430616,4.56683470602801,333.169146150116));
#26129=CARTESIAN_POINT('Ctrl Pts',(16.5075448646838,4.51395217585439,333.042386617226));
#26130=CARTESIAN_POINT('Ctrl Pts',(16.4997977863059,4.45586261669995,332.918060662844));
#26131=CARTESIAN_POINT('Ctrl Pts',(16.4920506430001,4.39777257069912,332.793733666492));
#26132=CARTESIAN_POINT('Ctrl Pts',(16.4843034996943,4.33447557413499,332.671840643454));
#26133=CARTESIAN_POINT('Ctrl Pts',(16.4765563563885,4.26621365285367,332.552837534877));
#26134=CARTESIAN_POINT('Ctrl Pts',(16.4688074713604,4.19793638484321,332.433807671876));
#26135=CARTESIAN_POINT('Ctrl Pts',(16.4610585863323,4.12469216540993,332.317669355183));
#26136=CARTESIAN_POINT('Ctrl Pts',(16.4533097013042,4.04676763725206,332.204851568773));
#26137=CARTESIAN_POINT('Ctrl Pts',(16.4455525915295,3.96876039919489,332.091914036399));
#26138=CARTESIAN_POINT('Ctrl Pts',(16.4377954817547,3.88606315140357,331.982304396841));
#26139=CARTESIAN_POINT('Ctrl Pts',(16.43003837198,3.79900465347133,331.876420850146));
#26140=CARTESIAN_POINT('Ctrl Pts',(16.4222771170538,3.71189963426132,331.770480722669));
#26141=CARTESIAN_POINT('Ctrl Pts',(16.4145158621276,3.62042898168615,331.668270946632));
#26142=CARTESIAN_POINT('Ctrl Pts',(16.4067546072014,3.52495930443916,331.570153798704));
#26143=CARTESIAN_POINT('Ctrl Pts',(16.3989809367968,3.42933690682208,331.471879695315));
#26144=CARTESIAN_POINT('Ctrl Pts',(16.3912072663921,3.32970298538194,331.377711571252));
#26145=CARTESIAN_POINT('Ctrl Pts',(16.3834335959875,3.22645895832361,331.287972837821));
#26146=CARTESIAN_POINT('Ctrl Pts',(16.3760217918105,3.1280209655656,331.202411464023));
#26147=CARTESIAN_POINT('Ctrl Pts',(16.3686099876335,3.02630162884219,331.120876564858));
#26148=CARTESIAN_POINT('Ctrl Pts',(16.3611981834565,2.92167277902398,331.043611339263));
#26149=CARTESIAN_POINT('Ctrl Pts',(16.3534231046781,2.81191575760143,330.962559114799));
#26150=CARTESIAN_POINT('Ctrl Pts',(16.3456480258997,2.69860995132663,330.885949545503));
#26151=CARTESIAN_POINT('Ctrl Pts',(16.3378729471213,2.58215078352836,330.814109366739));
#26152=CARTESIAN_POINT('Ctrl Pts',(16.3301074360723,2.46583492615005,330.742357591888));
#26153=CARTESIAN_POINT('Ctrl Pts',(16.3223419250233,2.3463737576461,330.675363733119));
#26154=CARTESIAN_POINT('Ctrl Pts',(16.3145764139743,2.22419457915933,330.613413452747));
#26155=CARTESIAN_POINT('Ctrl Pts',(16.3068186024521,2.102136541684,330.551524596259));
#26156=CARTESIAN_POINT('Ctrl Pts',(16.2990607909299,1.97736620363373,330.494669542076));
#26157=CARTESIAN_POINT('Ctrl Pts',(16.2913029794077,1.85033826544513,330.443089712763));
#26158=CARTESIAN_POINT('Ctrl Pts',(16.2835510058847,1.7234059198083,330.391548698907));
#26159=CARTESIAN_POINT('Ctrl Pts',(16.2757990323618,1.59421971634065,330.345275154742));
#26160=CARTESIAN_POINT('Ctrl Pts',(16.2680470588388,1.46325696151485,330.304463595384));
#26161=CARTESIAN_POINT('Ctrl Pts',(16.2602983682811,1.33234966949331,330.263669319744));
#26162=CARTESIAN_POINT('Ctrl Pts',(16.2525496777236,1.1996676949233,330.22833254426));
#26163=CARTESIAN_POINT('Ctrl Pts',(16.2448009871659,1.06570603275893,330.198598775957));
#26164=CARTESIAN_POINT('Ctrl Pts',(16.2370539087881,0.931772242437241,330.168871194013));
#26165=CARTESIAN_POINT('Ctrl Pts',(16.2293068304103,0.796559675458909,330.144744385128));
#26166=CARTESIAN_POINT('Ctrl Pts',(16.2215597520325,0.660575734404991,330.126313226969));
#26167=CARTESIAN_POINT('Ctrl Pts',(16.2138126087267,0.524590653674855,330.10788191434));
#26168=CARTESIAN_POINT('Ctrl Pts',(16.2060654654209,0.387834573307152,330.095146400147));
#26169=CARTESIAN_POINT('Ctrl Pts',(16.1983183221151,0.25082187801229,330.088149895609));
#26170=CARTESIAN_POINT('Ctrl Pts',(16.190569437087,0.113778379354477,330.081151818108));
#26171=CARTESIAN_POINT('Ctrl Pts',(16.1828205520589,-0.0235214587427138,
330.079895337648));
#26172=CARTESIAN_POINT('Ctrl Pts',(16.1750716670308,-0.160561775691114,
330.084371558113));
#26173=CARTESIAN_POINT('Ctrl Pts',(16.1673145572561,-0.297747548647628,
330.088852529685));
#26174=CARTESIAN_POINT('Ctrl Pts',(16.1595574474814,-0.434672858918308,
330.099078344256));
#26175=CARTESIAN_POINT('Ctrl Pts',(16.1518003377067,-0.570824940906885,
330.114988029765));
#26176=CARTESIAN_POINT('Ctrl Pts',(16.1440390827805,-0.70704977821487,330.130906216902));
#26177=CARTESIAN_POINT('Ctrl Pts',(16.1362778278544,-0.842500178127734,
330.152514265483));
#26178=CARTESIAN_POINT('Ctrl Pts',(16.1285165729282,-0.976673101465136,
330.179699935131));
#26179=CARTESIAN_POINT('Ctrl Pts',(16.1207429025236,-1.11106065775302,330.206929092991));
#26180=CARTESIAN_POINT('Ctrl Pts',(16.1129692321189,-1.24416627415039,330.23975360783));
#26181=CARTESIAN_POINT('Ctrl Pts',(16.1051955617142,-1.3755007567666,330.278010934931));
#26182=CARTESIAN_POINT('Ctrl Pts',(16.097783757537,-1.50072158762172,330.314487374251));
#26183=CARTESIAN_POINT('Ctrl Pts',(16.0903719533599,-1.62433219355919,330.35590212218));
#26184=CARTESIAN_POINT('Ctrl Pts',(16.0829601491827,-1.74592684438599,330.402074107105));
#26185=CARTESIAN_POINT('Ctrl Pts',(16.0751850704042,-1.87348121125986,330.45050911855));
#26186=CARTESIAN_POINT('Ctrl Pts',(16.0674099916258,-1.99922010573587,330.504332554518));
#26187=CARTESIAN_POINT('Ctrl Pts',(16.0596349128473,-2.12265478282301,330.563388710349));
#26188=CARTESIAN_POINT('Ctrl Pts',(16.0518694017983,-2.24593756568176,330.622372193821));
#26189=CARTESIAN_POINT('Ctrl Pts',(16.0441038907493,-2.36692142373041,330.686575417921));
#26190=CARTESIAN_POINT('Ctrl Pts',(16.0363383797003,-2.48513490026524,330.755793644274));
#26191=CARTESIAN_POINT('Ctrl Pts',(16.0285805681781,-2.60323116779383,330.824943240554));
#26192=CARTESIAN_POINT('Ctrl Pts',(16.0208227566559,-2.71856218504585,330.899097747518));
#26193=CARTESIAN_POINT('Ctrl Pts',(16.0130649451337,-2.83067887013833,330.978005445472));
#26194=CARTESIAN_POINT('Ctrl Pts',(16.0053129716106,-2.94271118387001,331.056853762881));
#26195=CARTESIAN_POINT('Ctrl Pts',(15.9975609980876,-3.05153366176024,331.140447927522));
#26196=CARTESIAN_POINT('Ctrl Pts',(15.9898090245646,-3.15672443397928,331.228491825487));
#26197=CARTESIAN_POINT('Ctrl Pts',(15.982060334007,-3.26187065784369,331.316498436809));
#26198=CARTESIAN_POINT('Ctrl Pts',(15.9743116434494,-3.36338793595524,331.408950783033));
#26199=CARTESIAN_POINT('Ctrl Pts',(15.9665629528917,-3.46088603817935,331.505511354542));
#26200=CARTESIAN_POINT('Ctrl Pts',(15.9588158745139,-3.55836385510897,331.602051835817));
#26201=CARTESIAN_POINT('Ctrl Pts',(15.951068796136,-3.65182388191053,331.70269856734));
#26202=CARTESIAN_POINT('Ctrl Pts',(15.9433217177582,-3.74091174927873,331.807076207203));
#26203=CARTESIAN_POINT('Ctrl Pts',(15.9355745744524,-3.83000036328894,331.911454721852));
#26204=CARTESIAN_POINT('Ctrl Pts',(15.9278274311466,-3.91471649102352,332.019563909902));
#26205=CARTESIAN_POINT('Ctrl Pts',(15.9200802878408,-3.99474543216421,332.130994598349));
#26206=CARTESIAN_POINT('Ctrl Pts',(15.9123314028127,-4.07479236550982,332.24245033878));
#26207=CARTESIAN_POINT('Ctrl Pts',(15.9045825177846,-4.15014978739144,332.357228748126));
#26208=CARTESIAN_POINT('Ctrl Pts',(15.8968336327565,-4.22054601697861,332.474891214014));
#26209=CARTESIAN_POINT('Ctrl Pts',(15.8890765229818,-4.29101696585138,332.592678568059));
#26210=CARTESIAN_POINT('Ctrl Pts',(15.8813194132071,-4.35651600238068,332.713355757661));
#26211=CARTESIAN_POINT('Ctrl Pts',(15.8735623034324,-4.4168169123865,332.836458591809));
#26212=CARTESIAN_POINT('Ctrl Pts',(15.8658010485062,-4.47715004527053,332.959627208176));
#26213=CARTESIAN_POINT('Ctrl Pts',(15.85803979358,-4.53227935976597,333.085223694128));
#26214=CARTESIAN_POINT('Ctrl Pts',(15.8502785386539,-4.58202701783645,333.212764293576));
#26215=CARTESIAN_POINT('Ctrl Pts',(15.8425048682492,-4.63185425594712,333.340508916418));
#26216=CARTESIAN_POINT('Ctrl Pts',(15.8347311978446,-4.67628250776983,333.47020349738));
#26217=CARTESIAN_POINT('Ctrl Pts',(15.8269575274399,-4.71518372974108,333.60134870061));
#26218=CARTESIAN_POINT('Ctrl Pts',(15.8195457232628,-4.75227409047033,333.726389063077));
#26219=CARTESIAN_POINT('Ctrl Pts',(15.8121339190857,-4.78434033703889,333.852747755207));
#26220=CARTESIAN_POINT('Ctrl Pts',(15.8047221149087,-4.81131517254095,333.979985601583));
#26221=CARTESIAN_POINT('Ctrl Pts',(15.7938135927537,-4.85101611224083,334.167251324341));
#26222=CARTESIAN_POINT('Ctrl Pts',(15.7829050705987,-4.87979520388835,334.356906926838));
#26223=CARTESIAN_POINT('Ctrl Pts',(15.7719965484437,-4.89742617354449,334.547893887255));
#26224=CARTESIAN_POINT('Ctrl Pts',(15.7635097817925,-4.91114296516664,334.696480629203));
#26225=CARTESIAN_POINT('Ctrl Pts',(15.7550230151414,-4.91811289450606,334.845873039927));
#26226=CARTESIAN_POINT('Ctrl Pts',(15.7465362484902,-4.91824799676507,334.99556098926));
#26227=CARTESIAN_POINT('',(19.2465362484902,-4.91524060940954,335.003192664787));
#26228=CARTESIAN_POINT('Ctrl Pts',(19.2465362484902,-4.91824896247744,335.003194618845));
#26229=CARTESIAN_POINT('Ctrl Pts',(19.2377820254298,-4.91814815424287,335.158393100778));
#26230=CARTESIAN_POINT('Ctrl Pts',(19.2290278023693,-4.91069724366754,335.313310701779));
#26231=CARTESIAN_POINT('Ctrl Pts',(19.2202735793088,-4.8960000081695,335.467297531027));
#26232=CARTESIAN_POINT('Ctrl Pts',(19.2114841097102,-4.88124359818296,335.621904347066));
#26233=CARTESIAN_POINT('Ctrl Pts',(19.2026946401115,-4.85918250561117,335.775572701174));
#26234=CARTESIAN_POINT('Ctrl Pts',(19.1939051705129,-4.82997157456934,335.927662466284));
#26235=CARTESIAN_POINT('Ctrl Pts',(19.1850664219562,-4.80059686979468,336.080604936449));
#26236=CARTESIAN_POINT('Ctrl Pts',(19.1762276733995,-4.76399202541037,336.231950888511));
#26237=CARTESIAN_POINT('Ctrl Pts',(19.1673889248429,-4.72036323075361,336.381069886809));
#26238=CARTESIAN_POINT('Ctrl Pts',(19.1594521252939,-4.68118653107344,336.514972055293));
#26239=CARTESIAN_POINT('Ctrl Pts',(19.1515153257449,-4.63634695919046,336.647078772111));
#26240=CARTESIAN_POINT('Ctrl Pts',(19.1435785261959,-4.58602598893983,336.776949265249));
#26241=CARTESIAN_POINT('Ctrl Pts',(19.1358034474176,-4.53673036222163,336.904173508333));
#26242=CARTESIAN_POINT('Ctrl Pts',(19.1280283686392,-4.48205869875328,337.029545917805));
#26243=CARTESIAN_POINT('Ctrl Pts',(19.1202532898608,-4.42217000146141,337.152578811722));
#26244=CARTESIAN_POINT('Ctrl Pts',(19.1124877788118,-4.36235500102435,337.27546030583));
#26245=CARTESIAN_POINT('Ctrl Pts',(19.1047222677628,-4.29733590994779,337.396007664526));
#26246=CARTESIAN_POINT('Ctrl Pts',(19.0969567567139,-4.2273206469613,337.513750825017));
#26247=CARTESIAN_POINT('Ctrl Pts',(19.0891989451918,-4.15737480431186,337.631377242822));
#26248=CARTESIAN_POINT('Ctrl Pts',(19.0814411336696,-4.08244284642495,337.746204661719));
#26249=CARTESIAN_POINT('Ctrl Pts',(19.0736833221475,-4.00277952111879,337.857785710618));
#26250=CARTESIAN_POINT('Ctrl Pts',(19.0659313486245,-3.92317614499119,337.969282791239));
#26251=CARTESIAN_POINT('Ctrl Pts',(19.0581793751016,-3.83884871465946,338.077538047691));
#26252=CARTESIAN_POINT('Ctrl Pts',(19.0504274015786,-3.75009618730341,338.182131620231));
#26253=CARTESIAN_POINT('Ctrl Pts',(19.042678711021,-3.66138124669539,338.28668089733));
#26254=CARTESIAN_POINT('Ctrl Pts',(19.0349300204635,-3.56824518875034,338.387571277386));
#26255=CARTESIAN_POINT('Ctrl Pts',(19.0271813299059,-3.47102815166506,338.484414819284));
#26256=CARTESIAN_POINT('Ctrl Pts',(19.0194342515281,-3.37383134139633,338.581238212076));
#26257=CARTESIAN_POINT('Ctrl Pts',(19.0116871731503,-3.27255551761854,338.674016165781));
#26258=CARTESIAN_POINT('Ctrl Pts',(19.0039400947726,-3.16757840768925,338.762396854884));
#26259=CARTESIAN_POINT('Ctrl Pts',(18.9961929514668,-3.06260041795096,338.850778284702));
#26260=CARTESIAN_POINT('Ctrl Pts',(18.9884458081611,-2.95392137920249,338.93476212467));
#26261=CARTESIAN_POINT('Ctrl Pts',(18.9806986648553,-2.84195258113796,339.014036445906));
#26262=CARTESIAN_POINT('Ctrl Pts',(18.9729497798273,-2.7299586101103,339.093328589693));
#26263=CARTESIAN_POINT('Ctrl Pts',(18.9652008947991,-2.61467372698004,339.167908882037));
#26264=CARTESIAN_POINT('Ctrl Pts',(18.9574520097711,-2.49653836950835,339.237508611445));
#26265=CARTESIAN_POINT('Ctrl Pts',(18.9496948999964,-2.37827762194752,339.307182214726));
#26266=CARTESIAN_POINT('Ctrl Pts',(18.9419377902218,-2.25716069358419,339.371864496226));
#26267=CARTESIAN_POINT('Ctrl Pts',(18.9341806804471,-2.13365329307323,339.431332382868));
#26268=CARTESIAN_POINT('Ctrl Pts',(18.926419425521,-2.01007989415652,339.490832047248));
#26269=CARTESIAN_POINT('Ctrl Pts',(18.9186581705949,-1.88411383655771,339.545111610003));
#26270=CARTESIAN_POINT('Ctrl Pts',(18.9108969156687,-1.75624006674755,339.593996505272));
#26271=CARTESIAN_POINT('Ctrl Pts',(18.9031232452641,-1.62816174057967,339.642959600442));
#26272=CARTESIAN_POINT('Ctrl Pts',(18.8953495748595,-1.49816997478634,339.686510659174));
#26273=CARTESIAN_POINT('Ctrl Pts',(18.8875759044549,-1.3667649588507,339.724525014195));
#26274=CARTESIAN_POINT('Ctrl Pts',(18.8801641002773,-1.24147687801078,339.760769791848));
#26275=CARTESIAN_POINT('Ctrl Pts',(18.8727522960996,-1.11490443906098,339.791981663734));
#26276=CARTESIAN_POINT('Ctrl Pts',(18.8653404919219,-0.987487262032757,
339.818096301427));
#26277=CARTESIAN_POINT('Ctrl Pts',(18.8575654131435,-0.853824989612378,
339.845490895302));
#26278=CARTESIAN_POINT('Ctrl Pts',(18.8497903343651,-0.718810681621633,
339.867362531755));
#26279=CARTESIAN_POINT('Ctrl Pts',(18.8420152555866,-0.582940485816961,
339.883581007058));
#26280=CARTESIAN_POINT('Ctrl Pts',(18.8342497445376,-0.447237486938147,
339.899779524494));
#26281=CARTESIAN_POINT('Ctrl Pts',(18.8264842334886,-0.310681080268791,
339.910338676482));
#26282=CARTESIAN_POINT('Ctrl Pts',(18.8187187224396,-0.173779068393592,
339.91517892837));
#26283=CARTESIAN_POINT('Ctrl Pts',(18.8109609109174,-0.0370127952616527,
339.920014381133));
#26284=CARTESIAN_POINT('Ctrl Pts',(18.8032030993952,0.100098013032427,339.919142204303));
#26285=CARTESIAN_POINT('Ctrl Pts',(18.795445287873,0.237039293933692,339.912534522589));
#26286=CARTESIAN_POINT('Ctrl Pts',(18.78769331435,0.373877522178236,339.905931813365));
#26287=CARTESIAN_POINT('Ctrl Pts',(18.779941340827,0.510546088113213,339.893602209103));
#26288=CARTESIAN_POINT('Ctrl Pts',(18.772189367304,0.646530139839806,339.875569899076));
#26289=CARTESIAN_POINT('Ctrl Pts',(18.7644406767464,0.782456602239759,339.857545225743));
#26290=CARTESIAN_POINT('Ctrl Pts',(18.7566919861888,0.917698740330531,339.833822701383));
#26291=CARTESIAN_POINT('Ctrl Pts',(18.7489432956312,1.0517462578595,339.804478418265));
#26292=CARTESIAN_POINT('Ctrl Pts',(18.7411962172533,1.18576588568286,339.775140240471));
#26293=CARTESIAN_POINT('Ctrl Pts',(18.7334491388756,1.31859100573686,339.740182713979));
#26294=CARTESIAN_POINT('Ctrl Pts',(18.7257020604978,1.44972135049144,339.699733084807));
#26295=CARTESIAN_POINT('Ctrl Pts',(18.717954917192,1.5808527942446,339.659283116628));
#26296=CARTESIAN_POINT('Ctrl Pts',(18.7102077738862,1.71028906085988,339.613341069176));
#26297=CARTESIAN_POINT('Ctrl Pts',(18.7024606305804,1.8375452702326,339.562084002114));
#26298=CARTESIAN_POINT('Ctrl Pts',(18.6947117455523,1.96483008950291,339.510815411375));
#26299=CARTESIAN_POINT('Ctrl Pts',(18.6869628605242,2.08993351374294,339.454229569258));
#26300=CARTESIAN_POINT('Ctrl Pts',(18.6792139754961,2.21239123158162,339.392551434067));
#26301=CARTESIAN_POINT('Ctrl Pts',(18.6714568657214,2.33497892730725,339.330807833065));
#26302=CARTESIAN_POINT('Ctrl Pts',(18.6636997559466,2.45491495738214,339.263961318076));
#26303=CARTESIAN_POINT('Ctrl Pts',(18.6559426461719,2.57175971322129,339.192282795799));
#26304=CARTESIAN_POINT('Ctrl Pts',(18.6481813912458,2.68866690716192,339.120565970812));
#26305=CARTESIAN_POINT('Ctrl Pts',(18.6404201363196,2.80247921118399,339.044012211576));
#26306=CARTESIAN_POINT('Ctrl Pts',(18.6326588813935,2.91278739676901,338.962934852319));
#26307=CARTESIAN_POINT('Ctrl Pts',(18.6248852109888,3.02327203950161,338.88172779571));
#26308=CARTESIAN_POINT('Ctrl Pts',(18.6171115405842,3.13024105730717,338.79598292344));
#26309=CARTESIAN_POINT('Ctrl Pts',(18.6093378701796,3.23331893358655,338.706053390901));
#26310=CARTESIAN_POINT('Ctrl Pts',(18.6019260660024,3.33159850992685,338.620310099737));
#26311=CARTESIAN_POINT('Ctrl Pts',(18.5945142618253,3.42634084830613,338.53076317034));
#26312=CARTESIAN_POINT('Ctrl Pts',(18.5871024576481,3.51725394995298,338.43774747677));
#26313=CARTESIAN_POINT('Ctrl Pts',(18.5793273788697,3.61262297352746,338.340172806979));
#26314=CARTESIAN_POINT('Ctrl Pts',(18.5715523000912,3.70407928840549,338.238472392464));
#26315=CARTESIAN_POINT('Ctrl Pts',(18.5637772213128,3.79124490947381,338.13299299375));
#26316=CARTESIAN_POINT('Ctrl Pts',(18.5560117102637,3.87830326769617,338.027643394151));
#26317=CARTESIAN_POINT('Ctrl Pts',(18.5482461992147,3.9610811911269,337.918524361504));
#26318=CARTESIAN_POINT('Ctrl Pts',(18.5404806881656,4.039236996263,337.806019877071));
#26319=CARTESIAN_POINT('Ctrl Pts',(18.5327228766434,4.11731530969082,337.693626941162));
#26320=CARTESIAN_POINT('Ctrl Pts',(18.5249650651211,4.19078040337237,337.577855552408));
#26321=CARTESIAN_POINT('Ctrl Pts',(18.5172072535989,4.25933064763511,337.45912291206));
#26322=CARTESIAN_POINT('Ctrl Pts',(18.5094552800758,4.32782930566519,337.340479621788));
#26323=CARTESIAN_POINT('Ctrl Pts',(18.5017033065528,4.39142028146919,337.218879852658));
#26324=CARTESIAN_POINT('Ctrl Pts',(18.4939513330297,4.44984530041762,337.094769644818));
#26325=CARTESIAN_POINT('Ctrl Pts',(18.4862026424721,4.50824557633576,336.970711997725));
#26326=CARTESIAN_POINT('Ctrl Pts',(18.4784539519145,4.56148408061635,336.84414637941));
#26327=CARTESIAN_POINT('Ctrl Pts',(18.4707052613568,4.60934865029003,336.715543086772));
#26328=CARTESIAN_POINT('Ctrl Pts',(18.4629581829789,4.65720326134028,336.586966551122));
#26329=CARTESIAN_POINT('Ctrl Pts',(18.455211104601,4.6996860254917,336.456353550521));
#26330=CARTESIAN_POINT('Ctrl Pts',(18.4474640262231,4.73663322317013,336.324193630728));
#26331=CARTESIAN_POINT('Ctrl Pts',(18.4397168829173,4.77358073050161,336.192032603308));
#26332=CARTESIAN_POINT('Ctrl Pts',(18.4319697396115,4.80499247358572,336.058325007279));
#26333=CARTESIAN_POINT('Ctrl Pts',(18.4242225963056,4.83075494922247,335.923574405807));
#26334=CARTESIAN_POINT('Ctrl Pts',(18.4164737112775,4.85652321681069,335.78879350954));
#26335=CARTESIAN_POINT('Ctrl Pts',(18.4087248262494,4.87663961625762,335.652969525067));
#26336=CARTESIAN_POINT('Ctrl Pts',(18.4009759412212,4.89104205427432,335.516614639572));
#26337=CARTESIAN_POINT('Ctrl Pts',(18.3932188314465,4.90545977918754,335.380115025593));
#26338=CARTESIAN_POINT('Ctrl Pts',(18.3854617216717,4.9141513864259,335.243083774266));
#26339=CARTESIAN_POINT('Ctrl Pts',(18.3777046118969,4.9171067897841,335.10603716499));
#26340=CARTESIAN_POINT('Ctrl Pts',(18.3699433569708,4.92006377241535,334.968917322388));
#26341=CARTESIAN_POINT('Ctrl Pts',(18.3621821020445,4.9172784513251,334.83178249608));
#26342=CARTESIAN_POINT('Ctrl Pts',(18.3544208471183,4.90879285891832,334.695146378187));
#26343=CARTESIAN_POINT('Ctrl Pts',(18.3466471767137,4.90029369232915,334.558291687035));
#26344=CARTESIAN_POINT('Ctrl Pts',(18.338873506309,4.8860760733654,334.421937687453));
#26345=CARTESIAN_POINT('Ctrl Pts',(18.3310998359043,4.86623376435236,334.286591272007));
#26346=CARTESIAN_POINT('Ctrl Pts',(18.3236880317275,4.84731511959862,334.157545264768));
#26347=CARTESIAN_POINT('Ctrl Pts',(18.3162762275508,4.82328371188101,334.029415429495));
#26348=CARTESIAN_POINT('Ctrl Pts',(18.308864423374,4.79426312665065,333.902628533751));
#26349=CARTESIAN_POINT('Ctrl Pts',(18.3010893445956,4.76382015608888,333.769627434562));
#26350=CARTESIAN_POINT('Ctrl Pts',(18.2933142658172,4.72779036758314,333.637683938384));
#26351=CARTESIAN_POINT('Ctrl Pts',(18.2855391870388,4.68626081002275,333.50730355298));
#26352=CARTESIAN_POINT('Ctrl Pts',(18.2777736759898,4.64478235722683,333.377083608942));
#26353=CARTESIAN_POINT('Ctrl Pts',(18.2700081649408,4.59781771888634,333.248423317326));
#26354=CARTESIAN_POINT('Ctrl Pts',(18.2622426538918,4.54550488848743,333.121817801374));
#26355=CARTESIAN_POINT('Ctrl Pts',(18.2544848423696,4.4932439264122,332.995337815159));
#26356=CARTESIAN_POINT('Ctrl Pts',(18.2467270308474,4.4356454733525,332.870908909159));
#26357=CARTESIAN_POINT('Ctrl Pts',(18.2389692193252,4.37289713361665,332.749010501733));
#26358=CARTESIAN_POINT('Ctrl Pts',(18.2312172458022,4.31019601399632,332.627203826725));
#26359=CARTESIAN_POINT('Ctrl Pts',(18.2234652722792,4.24235289977505,332.507924206048));
#26360=CARTESIAN_POINT('Ctrl Pts',(18.2157132987562,4.16960310840807,332.391630206268));
#26361=CARTESIAN_POINT('Ctrl Pts',(18.2079646081986,4.09688412662093,332.275385457065));
#26362=CARTESIAN_POINT('Ctrl Pts',(18.200215917641,4.01926280751208,332.162124144618));
#26363=CARTESIAN_POINT('Ctrl Pts',(18.1924672270834,3.93701982022087,332.052279185932));
#26364=CARTESIAN_POINT('Ctrl Pts',(18.1847201487056,3.85479394427009,331.942457081407));
#26365=CARTESIAN_POINT('Ctrl Pts',(18.1769730703277,3.7679485469018,331.836050229505));
#26366=CARTESIAN_POINT('Ctrl Pts',(18.1692259919499,3.67680669953446,331.733461226809));
#26367=CARTESIAN_POINT('Ctrl Pts',(18.1614788486441,3.58566408831078,331.630871364319));
#26368=CARTESIAN_POINT('Ctrl Pts',(18.1537317053383,3.49022521487238,331.532099707068));
#26369=CARTESIAN_POINT('Ctrl Pts',(18.1459845620325,3.39085211313526,331.437514209243));
#26370=CARTESIAN_POINT('Ctrl Pts',(18.1382356770045,3.29145667021513,331.34290744659));
#26371=CARTESIAN_POINT('Ctrl Pts',(18.1304867919763,3.18812552201458,331.252488985553));
#26372=CARTESIAN_POINT('Ctrl Pts',(18.1227379069483,3.08125577542158,331.16658821558));
#26373=CARTESIAN_POINT('Ctrl Pts',(18.1149807971735,2.97427259617522,331.080596269641));
#26374=CARTESIAN_POINT('Ctrl Pts',(18.1072236873988,2.86374362090279,330.999131838743));
#26375=CARTESIAN_POINT('Ctrl Pts',(18.0994665776241,2.75009754174042,330.922482792996));
#26376=CARTESIAN_POINT('Ctrl Pts',(18.0917053226979,2.63639073374697,330.84579278845));
#26377=CARTESIAN_POINT('Ctrl Pts',(18.0839440677718,2.51956383559806,330.773923501067));
#26378=CARTESIAN_POINT('Ctrl Pts',(18.0761828128456,2.40007156810452,330.707117573183));
#26379=CARTESIAN_POINT('Ctrl Pts',(18.068409142441,2.28038815192559,330.640204777586));
#26380=CARTESIAN_POINT('Ctrl Pts',(18.0606354720363,2.15803119526454,330.578371703528));
#26381=CARTESIAN_POINT('Ctrl Pts',(18.0528618016316,2.03347769506908,330.52181381292));
#26382=CARTESIAN_POINT('Ctrl Pts',(18.0454499974545,1.91472219027222,330.467888705726));
#26383=CARTESIAN_POINT('Ctrl Pts',(18.0380381932773,1.79397030461569,330.418758823205));
#26384=CARTESIAN_POINT('Ctrl Pts',(18.0306263891002,1.67164779522883,330.374551188133));
#26385=CARTESIAN_POINT('Ctrl Pts',(18.0228513103218,1.5433298952785,330.328176805177));
#26386=CARTESIAN_POINT('Ctrl Pts',(18.0150762315433,1.41287800850253,330.287072826296));
#26387=CARTESIAN_POINT('Ctrl Pts',(18.0073011527649,1.28076433431189,330.251439609476));
#26388=CARTESIAN_POINT('Ctrl Pts',(17.9995356417159,1.14881323440812,330.215850241598));
#26389=CARTESIAN_POINT('Ctrl Pts',(17.9917701306669,1.01520478970506,330.185718341606));
#26390=CARTESIAN_POINT('Ctrl Pts',(17.9840046196179,0.880430036092563,330.161195807429));
#26391=CARTESIAN_POINT('Ctrl Pts',(17.9762468080957,0.745788912040565,330.136697587416));
#26392=CARTESIAN_POINT('Ctrl Pts',(17.9684889965736,0.609984162461037,330.117797734637));
#26393=CARTESIAN_POINT('Ctrl Pts',(17.9607311850514,0.473520463938446,330.104597929411));
#26394=CARTESIAN_POINT('Ctrl Pts',(17.9529792115284,0.337159458676692,330.091408057456));
#26395=CARTESIAN_POINT('Ctrl Pts',(17.9452272380054,0.200140878988653,330.083909732563));
#26396=CARTESIAN_POINT('Ctrl Pts',(17.9374752644824,0.0629776870588596,
330.082153227943));
#26397=CARTESIAN_POINT('Ctrl Pts',(17.9297265739248,-0.0741274161777176,
330.080397467203));
#26398=CARTESIAN_POINT('Ctrl Pts',(17.9219778833672,-0.211376619818468,
330.084378695322));
#26399=CARTESIAN_POINT('Ctrl Pts',(17.9142291928096,-0.348253988541828,
330.094095167865));
#26400=CARTESIAN_POINT('Ctrl Pts',(17.9064821144318,-0.485102878785402,
330.103809618815));
#26401=CARTESIAN_POINT('Ctrl Pts',(17.898735036054,-0.621579698344404,330.119256913039));
#26402=CARTESIAN_POINT('Ctrl Pts',(17.8909879576762,-0.757171062679959,
330.140383241001));
#26403=CARTESIAN_POINT('Ctrl Pts',(17.8832408143704,-0.892763563401745,
330.161509746023));
#26404=CARTESIAN_POINT('Ctrl Pts',(17.8754936710645,-1.02747020788395,330.188315319542));
#26405=CARTESIAN_POINT('Ctrl Pts',(17.8677465277588,-1.16078565827567,330.220694640636));
#26406=CARTESIAN_POINT('Ctrl Pts',(17.8599976427307,-1.29413108081083,330.25308124129));
#26407=CARTESIAN_POINT('Ctrl Pts',(17.8522487577026,-1.42608430712066,330.291043990808));
#26408=CARTESIAN_POINT('Ctrl Pts',(17.8444998726745,-1.55615344927013,330.334427205066));
#26409=CARTESIAN_POINT('Ctrl Pts',(17.8367427628998,-1.68636064815112,330.377856466716));
#26410=CARTESIAN_POINT('Ctrl Pts',(17.8289856531251,-1.8146793967322,330.426717562068));
#26411=CARTESIAN_POINT('Ctrl Pts',(17.8212285433504,-1.94063562898163,330.480805777793));
#26412=CARTESIAN_POINT('Ctrl Pts',(17.8134672884243,-2.06665916821419,330.534922896532));
#26413=CARTESIAN_POINT('Ctrl Pts',(17.8057060334981,-2.19031732335299,330.594272532315));
#26414=CARTESIAN_POINT('Ctrl Pts',(17.797944778572,-2.31115997575782,330.658603608405));
#26415=CARTESIAN_POINT('Ctrl Pts',(17.7901711081674,-2.43219593702396,330.723037593251));
#26416=CARTESIAN_POINT('Ctrl Pts',(17.7823974377627,-2.55040705824079,330.792468744124));
#26417=CARTESIAN_POINT('Ctrl Pts',(17.7746237673581,-2.6653708408966,330.866601719771));
#26418=CARTESIAN_POINT('Ctrl Pts',(17.7672119631808,-2.77498303181388,330.937283787569));
#26419=CARTESIAN_POINT('Ctrl Pts',(17.7598001590035,-2.88164317223758,331.012239625843));
#26420=CARTESIAN_POINT('Ctrl Pts',(17.7523883548263,-2.98501404439358,331.091179945652));
#26421=CARTESIAN_POINT('Ctrl Pts',(17.7446981896833,-3.09226715832335,331.173084982705));
#26422=CARTESIAN_POINT('Ctrl Pts',(17.7370080245404,-3.19633425613697,331.259551070327));
#26423=CARTESIAN_POINT('Ctrl Pts',(17.7293178593975,-3.29679629098358,331.350299015226));
#26424=CARTESIAN_POINT('Ctrl Pts',(17.7216371958659,-3.39713419959996,331.440934836175));
#26425=CARTESIAN_POINT('Ctrl Pts',(17.7139565323343,-3.49387561020263,331.535841726835));
#26426=CARTESIAN_POINT('Ctrl Pts',(17.7062758688027,-3.58663160249314,331.634698110051));
#26427=CARTESIAN_POINT('Ctrl Pts',(17.6986027592911,-3.67929636820951,331.733457266888));
#26428=CARTESIAN_POINT('Ctrl Pts',(17.6909296497795,-3.76798324088064,331.836157899318));
#26429=CARTESIAN_POINT('Ctrl Pts',(17.6832565402679,-3.8523378461597,331.942439504843));
#26430=CARTESIAN_POINT('Ctrl Pts',(17.675476528112,-3.93786768950227,332.050201837921));
#26431=CARTESIAN_POINT('Ctrl Pts',(17.6676965159562,-4.01894332084126,332.161645408501));
#26432=CARTESIAN_POINT('Ctrl Pts',(17.6599165038003,-4.09523512542224,332.276356790986));
#26433=CARTESIAN_POINT('Ctrl Pts',(17.6522520831132,-4.17039342512254,332.389363850017));
#26434=CARTESIAN_POINT('Ctrl Pts',(17.6445876624261,-4.24090884870029,332.505541937));
#26435=CARTESIAN_POINT('Ctrl Pts',(17.636923241739,-4.30650827370955,332.62446436546));
#26436=CARTESIAN_POINT('Ctrl Pts',(17.6292600812692,-4.37209691257695,332.743367240178));
#26437=CARTESIAN_POINT('Ctrl Pts',(17.6215969207994,-4.43277096720742,332.865013208622));
#26438=CARTESIAN_POINT('Ctrl Pts',(17.6139337603296,-4.48830250834948,332.988949613748));
#26439=CARTESIAN_POINT('Ctrl Pts',(17.6062701133666,-4.54383757489307,333.112893886936));
#26440=CARTESIAN_POINT('Ctrl Pts',(17.5986064664036,-4.59422931560304,333.239128520474));
#26441=CARTESIAN_POINT('Ctrl Pts',(17.5909428194406,-4.6392975427444,333.367179932636));
#26442=CARTESIAN_POINT('Ctrl Pts',(17.5830756051977,-4.68556290441595,333.498632738127));
#26443=CARTESIAN_POINT('Ctrl Pts',(17.5752083909549,-4.72621782478933,333.631999771804));
#26444=CARTESIAN_POINT('Ctrl Pts',(17.567341176712,-4.76112199612357,333.766752092834));
#26445=CARTESIAN_POINT('Ctrl Pts',(17.559667529958,-4.79516737391469,333.898188924088));
#26446=CARTESIAN_POINT('Ctrl Pts',(17.5519938832039,-4.82374166199152,334.030943261726));
#26447=CARTESIAN_POINT('Ctrl Pts',(17.5443202364499,-4.84676671799636,334.164514845241));
#26448=CARTESIAN_POINT('Ctrl Pts',(17.5363562384626,-4.87066298343003,334.303140437005));
#26449=CARTESIAN_POINT('Ctrl Pts',(17.5283922404754,-4.88858176185565,334.442645856072));
#26450=CARTESIAN_POINT('Ctrl Pts',(17.5204282424881,-4.90049490263877,334.582468238679));
#26451=CARTESIAN_POINT('Ctrl Pts',(17.5124642445009,-4.9124080434219,334.722290621287));
#26452=CARTESIAN_POINT('Ctrl Pts',(17.5045002465137,-4.91831559428542,334.862429490414));
#26453=CARTESIAN_POINT('Ctrl Pts',(17.4965362485264,-4.91824945026714,335.002325391798));
#26454=CARTESIAN_POINT('',(20.9965362484902,-4.91588657005344,334.996283340543));
#26455=CARTESIAN_POINT('Ctrl Pts',(20.9965362484902,-4.91335673246954,334.996285253228));
#26456=CARTESIAN_POINT('Ctrl Pts',(20.93535974294,-4.90577737037676,336.078961636048));
#26457=CARTESIAN_POINT('Ctrl Pts',(20.7814372259651,-4.01911395901492,338.81429986906));
#26458=CARTESIAN_POINT('Ctrl Pts',(20.5347686975656,0.506096686042567,340.793816963868));
#26459=CARTESIAN_POINT('Ctrl Pts',(20.2565306632917,5.14602224722042,337.709779307904));
#26460=CARTESIAN_POINT('Ctrl Pts',(19.9782926290177,5.06351914728795,332.139017177353));
#26461=CARTESIAN_POINT('Ctrl Pts',(19.7000545947439,0.334299263309442,329.193736755108));
#26462=CARTESIAN_POINT('Ctrl Pts',(19.4561358012346,-4.08053706494637,331.282842392461));
#26463=CARTESIAN_POINT('Ctrl Pts',(19.3049630191501,-4.90617418397033,333.968623571676));
#26464=CARTESIAN_POINT('Ctrl Pts',(19.2465362484902,-4.91230824065646,335.003190760085));
#26465=CARTESIAN_POINT('',(22.7465362484346,-4.91824976548729,334.998481189866));
#26466=CARTESIAN_POINT('Ctrl Pts',(22.7465362484345,-4.91824976548729,334.998481189866));
#26467=CARTESIAN_POINT('Ctrl Pts',(22.7388226837815,-4.91829158424431,335.133899756872));
#26468=CARTESIAN_POINT('Ctrl Pts',(22.7311091191285,-4.91273627149401,335.269545225059));
#26469=CARTESIAN_POINT('Ctrl Pts',(22.7233955544755,-4.90155375923713,335.404912098866));
#26470=CARTESIAN_POINT('Ctrl Pts',(22.7156912571,-4.89038468194175,335.540116339386));
#26471=CARTESIAN_POINT('Ctrl Pts',(22.7079869597246,-4.87360188545452,335.675042258912));
#26472=CARTESIAN_POINT('Ctrl Pts',(22.7002826623491,-4.85122728219769,335.809182871149));
#26473=CARTESIAN_POINT('Ctrl Pts',(22.6925857063339,-4.82887399951244,335.943195661923));
#26474=CARTESIAN_POINT('Ctrl Pts',(22.6848887503186,-4.80093957597117,336.076424244487));
#26475=CARTESIAN_POINT('Ctrl Pts',(22.6771917943034,-4.76749780895062,336.208365716226));
#26476=CARTESIAN_POINT('Ctrl Pts',(22.6695002608708,-4.73407960198986,336.340214233877));
#26477=CARTESIAN_POINT('Ctrl Pts',(22.6618087274382,-4.69516186991169,336.470777061206));
#26478=CARTESIAN_POINT('Ctrl Pts',(22.6541171940056,-4.65086959118823,336.599560911082));
#26479=CARTESIAN_POINT('Ctrl Pts',(22.6464283535761,-4.6065928203277,336.728299670428));
#26480=CARTESIAN_POINT('Ctrl Pts',(22.6387395131467,-4.55694537205061,336.855260314972));
#26481=CARTESIAN_POINT('Ctrl Pts',(22.6310506727172,-4.50210216042523,336.979964444023));
#26482=CARTESIAN_POINT('Ctrl Pts',(22.623362963651,-4.44726701862451,337.104650223666));
#26483=CARTESIAN_POINT('Ctrl Pts',(22.6156752545848,-4.38723779378876,337.227079784249));
#26484=CARTESIAN_POINT('Ctrl Pts',(22.6079875455186,-4.3222374516481,337.346794936519));
#26485=CARTESIAN_POINT('Ctrl Pts',(22.6002992388898,-4.25723205705667,337.466519394199));
#26486=CARTESIAN_POINT('Ctrl Pts',(22.592610932261,-4.18725496639923,337.583528674518));
#26487=CARTESIAN_POINT('Ctrl Pts',(22.5849226256322,-4.11257474635776,337.697389852824));
#26488=CARTESIAN_POINT('Ctrl Pts',(22.5772319923915,-4.03787192681524,337.811285487455));
#26489=CARTESIAN_POINT('Ctrl Pts',(22.5695413591507,-3.95846336496409,337.922030792913));
#26490=CARTESIAN_POINT('Ctrl Pts',(22.56185072591,-3.87466023386913,338.029222859839));
#26491=CARTESIAN_POINT('Ctrl Pts',(22.5541517580921,-3.79076628272903,338.136531094124));
#26492=CARTESIAN_POINT('Ctrl Pts',(22.5464527902743,-3.70246849964301,338.240278088986));
#26493=CARTESIAN_POINT('Ctrl Pts',(22.5387538224564,-3.61011775775866,338.340094734826));
#26494=CARTESIAN_POINT('Ctrl Pts',(22.5310500850703,-3.51770980389792,338.439973217826));
#26495=CARTESIAN_POINT('Ctrl Pts',(22.5233463476842,-3.42124417273066,338.535916223746));
#26496=CARTESIAN_POINT('Ctrl Pts',(22.5156426102981,-3.32110679916533,338.627593236712));
#26497=CARTESIAN_POINT('Ctrl Pts',(22.5079277137406,-3.22082437261341,338.719403047494));
#26498=CARTESIAN_POINT('Ctrl Pts',(22.5002128171831,-3.11685988912234,338.80693427421));
#26499=CARTESIAN_POINT('Ctrl Pts',(22.4924979206257,-3.00963069273072,338.889897962142));
#26500=CARTESIAN_POINT('Ctrl Pts',(22.4891435929115,-2.96300895742366,338.925969398178));
#26501=CARTESIAN_POINT('Ctrl Pts',(22.4857892651973,-2.91577041472595,338.961177961164));
#26502=CARTESIAN_POINT('Ctrl Pts',(22.4824349374831,-2.86795086611008,338.995502583165));
#26503=CARTESIAN_POINT('Ctrl Pts',(22.4746598587047,-2.75710875725285,339.075064469431));
#26504=CARTESIAN_POINT('Ctrl Pts',(22.4668847799262,-2.64277821270163,339.15013615801));
#26505=CARTESIAN_POINT('Ctrl Pts',(22.4591097011478,-2.52535903425054,339.22039628597));
#26506=CARTESIAN_POINT('Ctrl Pts',(22.4513441900988,-2.40808434757379,339.29056995437));
#26507=CARTESIAN_POINT('Ctrl Pts',(22.4435786790498,-2.28772892162752,339.355943644326));
#26508=CARTESIAN_POINT('Ctrl Pts',(22.4358131680008,-2.16472387816742,339.416237492911));
#26509=CARTESIAN_POINT('Ctrl Pts',(22.4280553564786,-2.04184079456628,339.476471559969));
#26510=CARTESIAN_POINT('Ctrl Pts',(22.4202975449565,-1.91631367025211,339.531635637998));
#26511=CARTESIAN_POINT('Ctrl Pts',(22.4125397334343,-1.78860042604498,339.581494469979));
#26512=CARTESIAN_POINT('Ctrl Pts',(22.4047877599113,-1.66098329010396,339.631315781608));
#26513=CARTESIAN_POINT('Ctrl Pts',(22.3970357863883,-1.53118367145477,339.675839652223));
#26514=CARTESIAN_POINT('Ctrl Pts',(22.3892838128653,-1.3996814611181,339.714878033407));
#26515=CARTESIAN_POINT('Ctrl Pts',(22.3815351223077,-1.26823494204559,339.753899881813));
#26516=CARTESIAN_POINT('Ctrl Pts',(22.3737864317501,-1.13508763933206,339.78744075028));
#26517=CARTESIAN_POINT('Ctrl Pts',(22.3660377411925,-1.00073646871108,339.815361832998));
#26518=CARTESIAN_POINT('Ctrl Pts',(22.3582906628147,-0.866413250973457,
339.843277106501));
#26519=CARTESIAN_POINT('Ctrl Pts',(22.3505435844368,-0.73088704599748,339.86557484048));
#26520=CARTESIAN_POINT('Ctrl Pts',(22.342796506059,-0.594666491951997,339.882167021503));
#26521=CARTESIAN_POINT('Ctrl Pts',(22.3350493627532,-0.458444796246882,
339.898759341584));
#26522=CARTESIAN_POINT('Ctrl Pts',(22.3273022194474,-0.321529127871818,
339.909645966073));
#26523=CARTESIAN_POINT('Ctrl Pts',(22.3195550761416,-0.184434408416318,
339.914790637605));
#26524=CARTESIAN_POINT('Ctrl Pts',(22.3118061911135,-0.0473088671574665,
339.919936465769));
#26525=CARTESIAN_POINT('Ctrl Pts',(22.3040573060855,0.0899954147607131,
339.919337757548));
#26526=CARTESIAN_POINT('Ctrl Pts',(22.2963084210574,0.226962744033899,339.9130103781));
#26527=CARTESIAN_POINT('Ctrl Pts',(22.2885513112826,0.364075451845699,339.906676282706));
#26528=CARTESIAN_POINT('Ctrl Pts',(22.280794201508,0.500850101508433,339.89460138784));
#26529=CARTESIAN_POINT('Ctrl Pts',(22.2730370917332,0.636774798031272,339.876853588031));
#26530=CARTESIAN_POINT('Ctrl Pts',(22.2652758368071,0.772772128365996,339.859096304366));
#26531=CARTESIAN_POINT('Ctrl Pts',(22.2575145818808,0.90791821561975,339.835660142135));
#26532=CARTESIAN_POINT('Ctrl Pts',(22.2497533269547,1.04171158302198,339.806664128093));
#26533=CARTESIAN_POINT('Ctrl Pts',(22.24197965655,1.17571897620871,339.777621729878));
#26534=CARTESIAN_POINT('Ctrl Pts',(22.2342059861454,1.3083689470043,339.743001805863));
#26535=CARTESIAN_POINT('Ctrl Pts',(22.2264323157407,1.43917454233185,339.702973495482));
#26536=CARTESIAN_POINT('Ctrl Pts',(22.2190205115635,1.56389110572832,339.664808512579));
#26537=CARTESIAN_POINT('Ctrl Pts',(22.2116087073864,1.68693086912867,339.621727427768));
#26538=CARTESIAN_POINT('Ctrl Pts',(22.2041969032093,1.80789058585415,339.573916778001));
#26539=CARTESIAN_POINT('Ctrl Pts',(22.1964218244308,1.93477889861557,339.523762785869));
#26540=CARTESIAN_POINT('Ctrl Pts',(22.1886467456524,2.05977910106734,339.468245390123));
#26541=CARTESIAN_POINT('Ctrl Pts',(22.1808716668739,2.18240459657439,339.4075268847));
#26542=CARTESIAN_POINT('Ctrl Pts',(22.1731061558249,2.30487919360266,339.346883097263));
#26543=CARTESIAN_POINT('Ctrl Pts',(22.1653406447759,2.42498455114582,339.281051106691));
#26544=CARTESIAN_POINT('Ctrl Pts',(22.1575751337269,2.54225202177826,339.210242002577));
#26545=CARTESIAN_POINT('Ctrl Pts',(22.1498173222047,2.65940322137208,339.139503105896));
#26546=CARTESIAN_POINT('Ctrl Pts',(22.1420595106824,2.77372180117237,339.063797116992));
#26547=CARTESIAN_POINT('Ctrl Pts',(22.1343016991602,2.88476212130198,338.98338180018));
#26548=CARTESIAN_POINT('Ctrl Pts',(22.1265497256372,2.99571888006969,338.903026998443));
#26549=CARTESIAN_POINT('Ctrl Pts',(22.1187977521141,3.10340197429674,338.817970151135));
#26550=CARTESIAN_POINT('Ctrl Pts',(22.1110457785911,3.20739357349057,338.728513045067));
#26551=CARTESIAN_POINT('Ctrl Pts',(22.1032970880335,3.31134113217999,338.639093824136));
#26552=CARTESIAN_POINT('Ctrl Pts',(22.0955483974758,3.41160000952578,338.545278305213));
#26553=CARTESIAN_POINT('Ctrl Pts',(22.0877997069182,3.50778457114477,338.447409239551));
#26554=CARTESIAN_POINT('Ctrl Pts',(22.0800526285404,3.60394912076236,338.349560536365));
#26555=CARTESIAN_POINT('Ctrl Pts',(22.0723055501626,3.69604076697099,338.247660242575));
#26556=CARTESIAN_POINT('Ctrl Pts',(22.0645584717847,3.78371024409984,338.142088453751));
#26557=CARTESIAN_POINT('Ctrl Pts',(22.0568113284789,3.87138045598336,338.036515780133));
#26558=CARTESIAN_POINT('Ctrl Pts',(22.0490641851731,3.95462817514892,337.927271850814));
#26559=CARTESIAN_POINT('Ctrl Pts',(22.0413170418673,4.03314425838771,337.814770053403));
#26560=CARTESIAN_POINT('Ctrl Pts',(22.0335681568392,4.11167799370896,337.7022429632));
#26561=CARTESIAN_POINT('Ctrl Pts',(22.0258192718111,4.18547775265751,337.586456867904));
#26562=CARTESIAN_POINT('Ctrl Pts',(22.018070386783,4.25427780534426,337.467854010564));
#26563=CARTESIAN_POINT('Ctrl Pts',(22.0103132770083,4.32315088311768,337.349125266925));
#26564=CARTESIAN_POINT('Ctrl Pts',(22.0025561672335,4.38701345747788,337.227574127595));
#26565=CARTESIAN_POINT('Ctrl Pts',(21.9947990574588,4.44564560663194,337.103667797618));
#26566=CARTESIAN_POINT('Ctrl Pts',(21.9870378025326,4.50430908693178,336.97969525606));
#26567=CARTESIAN_POINT('Ctrl Pts',(21.9792765476065,4.55773642061718,336.853365375923));
#26568=CARTESIAN_POINT('Ctrl Pts',(21.9715152926804,4.60575632196914,336.725164271929));
#26569=CARTESIAN_POINT('Ctrl Pts',(21.9637416222757,4.65385303951368,336.596758087949));
#26570=CARTESIAN_POINT('Ctrl Pts',(21.955967951871,4.69652491747625,336.466475070168));
#26571=CARTESIAN_POINT('Ctrl Pts',(21.9481942814664,4.73365067056552,336.334816238871));
#26572=CARTESIAN_POINT('Ctrl Pts',(21.9407824772894,4.76904821091614,336.209286157848));
#26573=CARTESIAN_POINT('Ctrl Pts',(21.9333706731123,4.79940428359922,336.082505748886));
#26574=CARTESIAN_POINT('Ctrl Pts',(21.9259588689353,4.82465753160155,335.954915056568));
#26575=CARTESIAN_POINT('Ctrl Pts',(21.9181837901569,4.85114851651438,335.821070764345));
#26576=CARTESIAN_POINT('Ctrl Pts',(21.9104087113785,4.87210753607659,335.685911778915));
#26577=CARTESIAN_POINT('Ctrl Pts',(21.9026336326,4.88740774136202,335.549935116332));
#26578=CARTESIAN_POINT('Ctrl Pts',(21.894868121551,4.90268911877077,335.414125781688));
#26579=CARTESIAN_POINT('Ctrl Pts',(21.887102610502,4.91232549404534,335.277501156657));
#26580=CARTESIAN_POINT('Ctrl Pts',(21.879337099453,4.91624076491548,335.140569569549));
#26581=CARTESIAN_POINT('Ctrl Pts',(21.8715792879308,4.92015215378314,335.003773750509));
#26582=CARTESIAN_POINT('Ctrl Pts',(21.8638214764086,4.91835371572585,334.86667196327));
#26583=CARTESIAN_POINT('Ctrl Pts',(21.8560636648864,4.91082104894698,334.729778446975));
#26584=CARTESIAN_POINT('Ctrl Pts',(21.8483116913633,4.90329405073872,334.592987947391));
#26585=CARTESIAN_POINT('Ctrl Pts',(21.8405597178403,4.89004143437069,334.456405795499));
#26586=CARTESIAN_POINT('Ctrl Pts',(21.8328077443173,4.87109086675438,334.320546668032));
#26587=CARTESIAN_POINT('Ctrl Pts',(21.8250590537597,4.85214832471475,334.184745076987));
#26588=CARTESIAN_POINT('Ctrl Pts',(21.817310363202,4.82751268477103,334.049666287675));
#26589=CARTESIAN_POINT('Ctrl Pts',(21.8095616726444,4.79726348487193,333.915820070646));
#26590=CARTESIAN_POINT('Ctrl Pts',(21.8018145942665,4.76702057857156,333.782001701441));
#26591=CARTESIAN_POINT('Ctrl Pts',(21.7940675158888,4.73116652155738,333.649415775447));
#26592=CARTESIAN_POINT('Ctrl Pts',(21.7863204375109,4.68983193660753,333.518561689143));
#26593=CARTESIAN_POINT('Ctrl Pts',(21.7785732942051,4.64849700523404,333.387706506154));
#26594=CARTESIAN_POINT('Ctrl Pts',(21.7708261508993,4.60168157204609,333.258583564526));
#26595=CARTESIAN_POINT('Ctrl Pts',(21.7630790075935,4.54956596837533,333.131676537133));
#26596=CARTESIAN_POINT('Ctrl Pts',(21.7553301225654,4.49743864801056,333.004740978345));
#26597=CARTESIAN_POINT('Ctrl Pts',(21.7475812375373,4.44000893448496,332.880022686628));
#26598=CARTESIAN_POINT('Ctrl Pts',(21.7398323525093,4.3775049177217,332.757984443002));
#26599=CARTESIAN_POINT('Ctrl Pts',(21.7320752427345,4.314934558549,332.635816666722));
#26600=CARTESIAN_POINT('Ctrl Pts',(21.7243181329597,4.24727931572631,332.5163349694));
#26601=CARTESIAN_POINT('Ctrl Pts',(21.716561023185,4.17481305964195,332.399977119419));
#26602=CARTESIAN_POINT('Ctrl Pts',(21.7087997682588,4.10230807990751,332.283557091524));
#26603=CARTESIAN_POINT('Ctrl Pts',(21.7010385133327,4.02498718448782,332.170264559857));
#26604=CARTESIAN_POINT('Ctrl Pts',(21.6932772584065,3.94316646509159,332.060506626802));
#26605=CARTESIAN_POINT('Ctrl Pts',(21.6855035880019,3.86121485920964,331.950573116823));
#26606=CARTESIAN_POINT('Ctrl Pts',(21.6777299175972,3.77474929176875,331.844185807721));
#26607=CARTESIAN_POINT('Ctrl Pts',(21.6699562471925,3.68412544698488,331.741717821707));
#26608=CARTESIAN_POINT('Ctrl Pts',(21.6625444430155,3.59772016397853,331.644019745096));
#26609=CARTESIAN_POINT('Ctrl Pts',(21.6551326388384,3.50753522609962,331.549884522009));
#26610=CARTESIAN_POINT('Ctrl Pts',(21.6477208346613,3.41390747242586,331.459601882243));
#26611=CARTESIAN_POINT('Ctrl Pts',(21.6399457558829,3.31569074364166,331.364894221364));
#26612=CARTESIAN_POINT('Ctrl Pts',(21.6321706771044,3.21337479741648,331.274127052236));
#26613=CARTESIAN_POINT('Ctrl Pts',(21.6243955983259,3.1073089399203,331.187676008733));
#26614=CARTESIAN_POINT('Ctrl Pts',(21.6166300872769,3.0013736032144,331.101331348742));
#26615=CARTESIAN_POINT('Ctrl Pts',(21.6088645762279,2.89169783686368,331.019292491067));
#26616=CARTESIAN_POINT('Ctrl Pts',(21.6010990651789,2.77866792168339,330.941898517347));
#26617=CARTESIAN_POINT('Ctrl Pts',(21.5933412536567,2.66575007599316,330.864581279978));
#26618=CARTESIAN_POINT('Ctrl Pts',(21.5855834421345,2.54948502013865,330.791899980934));
#26619=CARTESIAN_POINT('Ctrl Pts',(21.5778256306123,2.43029198357238,330.724153424515));
#26620=CARTESIAN_POINT('Ctrl Pts',(21.5700736570893,2.31118864354578,330.656457849528));
#26621=CARTESIAN_POINT('Ctrl Pts',(21.5623216835663,2.18916204701557,330.593689817893));
#26622=CARTESIAN_POINT('Ctrl Pts',(21.5545697100433,2.06465996878092,330.536104585027));
#26623=CARTESIAN_POINT('Ctrl Pts',(21.5468210194857,1.94021061725066,330.478543739542));
#26624=CARTESIAN_POINT('Ctrl Pts',(21.5390723289281,1.81328822317247,330.426161491033));
#26625=CARTESIAN_POINT('Ctrl Pts',(21.5313236383705,1.68436450602539,330.379166820438));
#26626=CARTESIAN_POINT('Ctrl Pts',(21.5235765599926,1.55546761253445,330.332181927477));
#26627=CARTESIAN_POINT('Ctrl Pts',(21.5158294816148,1.42457059121446,330.290582516599));
#26628=CARTESIAN_POINT('Ctrl Pts',(21.5080824032369,1.29216408269702,330.254528996413));
#26629=CARTESIAN_POINT('Ctrl Pts',(21.5003352599311,1.15975646448497,330.218475174063));
#26630=CARTESIAN_POINT('Ctrl Pts',(21.4925881166253,1.02583971098499,330.187967437806));
#26631=CARTESIAN_POINT('Ctrl Pts',(21.4848409733195,0.890918140667847,330.163115886324));
#26632=CARTESIAN_POINT('Ctrl Pts',(21.4770920882914,0.75596623711778,330.138258747686));
#26633=CARTESIAN_POINT('Ctrl Pts',(21.4693432032633,0.620009451559208,330.119060395017));
#26634=CARTESIAN_POINT('Ctrl Pts',(21.4615943182352,0.483560378971694,330.105579459998));
#26635=CARTESIAN_POINT('Ctrl Pts',(21.4538372084605,0.346966477928753,330.092084216177));
#26636=CARTESIAN_POINT('Ctrl Pts',(21.4460800986857,0.209879635671917,330.084318550948));
#26637=CARTESIAN_POINT('Ctrl Pts',(21.438322988911,0.0728161879576935,330.082289062453));
#26638=CARTESIAN_POINT('Ctrl Pts',(21.4305617339849,-0.0643205020802697,
330.080258489464));
#26639=CARTESIAN_POINT('Ctrl Pts',(21.4228004790587,-0.201433382132718,
330.083970190382));
#26640=CARTESIAN_POINT('Ctrl Pts',(21.4150392241326,-0.338009055758815,
330.093378663405));
#26641=CARTESIAN_POINT('Ctrl Pts',(21.4072655537279,-0.474803205953177,
330.10280218692));
#26642=CARTESIAN_POINT('Ctrl Pts',(21.3994918833233,-0.611058043786753,
330.117940649785));
#26643=CARTESIAN_POINT('Ctrl Pts',(21.3917182129186,-0.746267321691431,
330.138696867395));
#26644=CARTESIAN_POINT('Ctrl Pts',(21.3843064087415,-0.875182575179624,
330.158486878082));
#26645=CARTESIAN_POINT('Ctrl Pts',(21.3768946045645,-1.00314713725636,330.183383345665));
#26646=CARTESIAN_POINT('Ctrl Pts',(21.3694828003874,-1.12973508500288,330.213259804396));
#26647=CARTESIAN_POINT('Ctrl Pts',(21.361707721609,-1.26252748515516,330.244600597366));
#26648=CARTESIAN_POINT('Ctrl Pts',(21.3539326428305,-1.39422456349755,330.281520935928));
#26649=CARTESIAN_POINT('Ctrl Pts',(21.3461575640521,-1.52432141188036,330.323930358112));
#26650=CARTESIAN_POINT('Ctrl Pts',(21.3383920530031,-1.65425816780887,330.366287592803));
#26651=CARTESIAN_POINT('Ctrl Pts',(21.3306265419541,-1.78259824381643,330.414120351281));
#26652=CARTESIAN_POINT('Ctrl Pts',(21.322861030905,-1.90884746020496,330.467287298298));
#26653=CARTESIAN_POINT('Ctrl Pts',(21.3151032193829,-2.03497150012728,330.520401530132));
#26654=CARTESIAN_POINT('Ctrl Pts',(21.3073454078607,-2.1590084480902,330.578839274642));
#26655=CARTESIAN_POINT('Ctrl Pts',(21.2995875963386,-2.28048016407282,330.642409692987));
#26656=CARTESIAN_POINT('Ctrl Pts',(21.2918356228156,-2.40186046873674,330.705932272577));
#26657=CARTESIAN_POINT('Ctrl Pts',(21.2840836492926,-2.52067903890204,330.774579657375));
#26658=CARTESIAN_POINT('Ctrl Pts',(21.2763316757697,-2.63647890820588,330.848113437353));
#26659=CARTESIAN_POINT('Ctrl Pts',(21.268582985212,-2.75222973619696,330.921616075733));
#26660=CARTESIAN_POINT('Ctrl Pts',(21.2608342946545,-2.86496407673566,331.000000784322));
#26661=CARTESIAN_POINT('Ctrl Pts',(21.2530856040969,-2.97425091881596,331.082983975726));
#26662=CARTESIAN_POINT('Ctrl Pts',(21.2453385257191,-3.08351502285583,331.165949901783));
#26663=CARTESIAN_POINT('Ctrl Pts',(21.2375914473412,-3.18933274405313,331.253512171376));
#26664=CARTESIAN_POINT('Ctrl Pts',(21.2298443689634,-3.2913036775886,331.345345000634));
#26665=CARTESIAN_POINT('Ctrl Pts',(21.2220972256576,-3.39327546573884,331.437178599539));
#26666=CARTESIAN_POINT('Ctrl Pts',(21.2143500823518,-3.49140011147154,331.533282567923));
#26667=CARTESIAN_POINT('Ctrl Pts',(21.206602939046,-3.58531211479375,331.633292394339));
#26668=CARTESIAN_POINT('Ctrl Pts',(21.1988540540179,-3.67924523152811,331.733324705088));
#26669=CARTESIAN_POINT('Ctrl Pts',(21.1911051689898,-3.76896355373146,331.837264336344));
#26670=CARTESIAN_POINT('Ctrl Pts',(21.1833562839617,-3.85414038221471,331.944711965022));
#26671=CARTESIAN_POINT('Ctrl Pts',(21.175599174187,-3.93940761826387,332.052273639723));
#26672=CARTESIAN_POINT('Ctrl Pts',(21.1678420644123,-4.02012348821465,332.163350442947));
#26673=CARTESIAN_POINT('Ctrl Pts',(21.1600849546375,-4.09600302464501,332.277511747574));
#26674=CARTESIAN_POINT('Ctrl Pts',(21.1523236997114,-4.17192310867353,332.391734056351));
#26675=CARTESIAN_POINT('Ctrl Pts',(21.1445624447852,-4.24300150711804,332.509043816707));
#26676=CARTESIAN_POINT('Ctrl Pts',(21.136801189859,-4.3089986551416,332.628984678985));
#26677=CARTESIAN_POINT('Ctrl Pts',(21.1290275194543,-4.37510137709339,332.749117407554));
#26678=CARTESIAN_POINT('Ctrl Pts',(21.1212538490497,-4.43610643175796,332.871889298458));
#26679=CARTESIAN_POINT('Ctrl Pts',(21.113480178645,-4.49182158413607,332.996822045152));
#26680=CARTESIAN_POINT('Ctrl Pts',(21.1060683744678,-4.54494318276729,333.115939142431));
#26681=CARTESIAN_POINT('Ctrl Pts',(21.0986565702907,-4.59325617917902,333.237020179856));
#26682=CARTESIAN_POINT('Ctrl Pts',(21.0912447661135,-4.63663642978742,333.359638551883));
#26683=CARTESIAN_POINT('Ctrl Pts',(21.0821717252757,-4.68973966564186,333.509739859241));
#26684=CARTESIAN_POINT('Ctrl Pts',(21.0730986844378,-4.7355897967023,333.662533588535));
#26685=CARTESIAN_POINT('Ctrl Pts',(21.0640256435999,-4.77394578823425,333.817365367706));
#26686=CARTESIAN_POINT('Ctrl Pts',(21.054991692469,-4.81213652927363,333.971530079576));
#26687=CARTESIAN_POINT('Ctrl Pts',(21.045957741338,-4.84289747739681,334.127715215526));
#26688=CARTESIAN_POINT('Ctrl Pts',(21.0369237902071,-4.86603740361971,334.285253157353));
#26689=CARTESIAN_POINT('Ctrl Pts',(21.0279628401055,-4.88899034206614,334.441518075698));
#26690=CARTESIAN_POINT('Ctrl Pts',(21.019001890004,-4.90444485114099,334.599113906424));
#26691=CARTESIAN_POINT('Ctrl Pts',(21.0100409399025,-4.91226154072782,334.757369379537));
#26692=CARTESIAN_POINT('Ctrl Pts',(21.0055393760983,-4.91618828136507,334.836869555467));
#26693=CARTESIAN_POINT('Ctrl Pts',(21.0010378122943,-4.91818830257432,334.916535897836));
#26694=CARTESIAN_POINT('Ctrl Pts',(20.9965362484902,-4.91824859433364,334.996281554732));
#26695=CARTESIAN_POINT('',(24.4965362484557,-4.91824791279987,335.004531085933));
#26696=CARTESIAN_POINT('Ctrl Pts',(24.4965362484557,-4.91824791279987,335.004531085932));
#26697=CARTESIAN_POINT('Ctrl Pts',(24.4864060560759,-4.91808312709539,335.183397026497));
#26698=CARTESIAN_POINT('Ctrl Pts',(24.4762758636962,-4.90815751266951,335.361829075815));
#26699=CARTESIAN_POINT('Ctrl Pts',(24.4661456713164,-4.88863305237369,335.538934079215));
#26700=CARTESIAN_POINT('Ctrl Pts',(24.455753395049,-4.86860346381701,335.720621065472));
#26701=CARTESIAN_POINT('Ctrl Pts',(24.4453611187817,-4.83847188859012,335.90091181959));
#26702=CARTESIAN_POINT('Ctrl Pts',(24.4349688425143,-4.79846090163957,336.07886794277));
#26703=CARTESIAN_POINT('Ctrl Pts',(24.4333462874764,-4.79221395181128,336.106652385441));
#26704=CARTESIAN_POINT('Ctrl Pts',(24.4317237324386,-4.78572626664462,336.134379960616));
#26705=CARTESIAN_POINT('Ctrl Pts',(24.4301011774008,-4.778998796945,336.162047142459));
#26706=CARTESIAN_POINT('Ctrl Pts',(24.4223260986224,-4.74676161196496,336.294624782907));
#26707=CARTESIAN_POINT('Ctrl Pts',(24.4145510198439,-4.7089524083983,336.426069432738));
#26708=CARTESIAN_POINT('Ctrl Pts',(24.4067759410655,-4.66566505716241,336.555876806458));
#26709=CARTESIAN_POINT('Ctrl Pts',(24.3990104300165,-4.62243097376797,336.685524443941));
#26710=CARTESIAN_POINT('Ctrl Pts',(24.3912449189675,-4.57373227824828,336.813538446878));
#26711=CARTESIAN_POINT('Ctrl Pts',(24.3834794079185,-4.51971364116093,336.939425601668));
#26712=CARTESIAN_POINT('Ctrl Pts',(24.3757215963963,-4.46574856370963,337.065187938977));
#26713=CARTESIAN_POINT('Ctrl Pts',(24.3679637848741,-4.40647419485819,337.188827267836));
#26714=CARTESIAN_POINT('Ctrl Pts',(24.3602059733519,-4.34208459926746,337.309866748387));
#26715=CARTESIAN_POINT('Ctrl Pts',(24.3524539998289,-4.27774345888933,337.430815142891));
#26716=CARTESIAN_POINT('Ctrl Pts',(24.3447020263059,-4.20829493659116,337.549167239647));
#26717=CARTESIAN_POINT('Ctrl Pts',(24.3369500527829,-4.13398052409446,337.66446769335));
#26718=CARTESIAN_POINT('Ctrl Pts',(24.3292013622253,-4.05969758379557,337.779719317243));
#26719=CARTESIAN_POINT('Ctrl Pts',(24.3214526716676,-3.98055306321583,337.891921540659));
#26720=CARTESIAN_POINT('Ctrl Pts',(24.31370398111,-3.89683345506705,338.000645278264));
#26721=CARTESIAN_POINT('Ctrl Pts',(24.3059569027322,-3.81313126548187,338.109346394988));
#26722=CARTESIAN_POINT('Ctrl Pts',(24.2982098243543,-3.72485612001893,338.214570155942));
#26723=CARTESIAN_POINT('Ctrl Pts',(24.2904627459765,-3.63233650013593,338.315918366347));
#26724=CARTESIAN_POINT('Ctrl Pts',(24.2827156026707,-3.53981610484941,338.417267426148));
#26725=CARTESIAN_POINT('Ctrl Pts',(24.2749684593649,-3.44305142772042,338.514740581938));
#26726=CARTESIAN_POINT('Ctrl Pts',(24.2672213160591,-3.34240944109033,338.607974804597));
#26727=CARTESIAN_POINT('Ctrl Pts',(24.259472431031,-3.24174482800509,338.70122998829));
#26728=CARTESIAN_POINT('Ctrl Pts',(24.2517235460029,-3.13720145751528,338.790244076901));
#26729=CARTESIAN_POINT('Ctrl Pts',(24.2439746609748,-3.02918085068011,338.874693076409));
#26730=CARTESIAN_POINT('Ctrl Pts',(24.2362175512001,-2.92104558965679,338.959231710958));
#26731=CARTESIAN_POINT('Ctrl Pts',(24.2284604414253,-2.80942602804438,339.039195336075));
#26732=CARTESIAN_POINT('Ctrl Pts',(24.2207033316506,-2.69475470829468,339.114301900034));
#26733=CARTESIAN_POINT('Ctrl Pts',(24.2129420767244,-2.58002211185827,339.189448598539));
#26734=CARTESIAN_POINT('Ctrl Pts',(24.2051808217983,-2.46223484333306,339.259732864015));
#26735=CARTESIAN_POINT('Ctrl Pts',(24.1974195668721,-2.34185086039195,339.324918220057));
#26736=CARTESIAN_POINT('Ctrl Pts',(24.1896458964675,-2.22127430231118,339.390207851425));
#26737=CARTESIAN_POINT('Ctrl Pts',(24.1818722260628,-2.09809308049226,339.450382102415));
#26738=CARTESIAN_POINT('Ctrl Pts',(24.1740985556581,-1.97278678925149,339.505251973714));
#26739=CARTESIAN_POINT('Ctrl Pts',(24.166686751481,-1.85331353601425,339.557567639304));
#26740=CARTESIAN_POINT('Ctrl Pts',(24.159274947304,-1.73190887298065,339.605061544593));
#26741=CARTESIAN_POINT('Ctrl Pts',(24.1518631431268,-1.60900023463661,339.647612430855));
#26742=CARTESIAN_POINT('Ctrl Pts',(24.1440880643483,-1.48006747780203,339.692248862805));
#26743=CARTESIAN_POINT('Ctrl Pts',(24.1363129855699,-1.34907213796948,339.731586539217));
#26744=CARTESIAN_POINT('Ctrl Pts',(24.1285379067915,-1.21648907850789,339.765431500334));
#26745=CARTESIAN_POINT('Ctrl Pts',(24.1207723957425,-1.08406917094163,339.79923481307));
#26746=CARTESIAN_POINT('Ctrl Pts',(24.1130068846935,-0.950065806337024,
339.827558763498));
#26747=CARTESIAN_POINT('Ctrl Pts',(24.1052413736444,-0.814972028073014,
339.850258101994));
#26748=CARTESIAN_POINT('Ctrl Pts',(24.0974835621223,-0.680012195683375,
339.87293493403));
#26749=CARTESIAN_POINT('Ctrl Pts',(24.0897257506001,-0.543964484168194,
339.889998187969));
#26750=CARTESIAN_POINT('Ctrl Pts',(24.0819679390779,-0.407334897859974,
339.901353011515));
#26751=CARTESIAN_POINT('Ctrl Pts',(24.0742159655549,-0.27080812964841,339.912699290196));
#26752=CARTESIAN_POINT('Ctrl Pts',(24.0664639920319,-0.133700746183982,
339.918345656773));
#26753=CARTESIAN_POINT('Ctrl Pts',(24.0587120185089,0.00347365792441432,
339.918248773314));
#26754=CARTESIAN_POINT('Ctrl Pts',(24.0509633279513,0.140589968591417,339.918151930884));
#26755=CARTESIAN_POINT('Ctrl Pts',(24.0432146373936,0.277772853389322,339.912316676307));
#26756=CARTESIAN_POINT('Ctrl Pts',(24.035465946836,0.414506447660042,339.90075172472));
#26757=CARTESIAN_POINT('Ctrl Pts',(24.0277188684582,0.551211593364265,339.889189179318));
#26758=CARTESIAN_POINT('Ctrl Pts',(24.0199717900804,0.687467245237846,339.871899341021));
#26759=CARTESIAN_POINT('Ctrl Pts',(24.0122247117026,0.822760792630141,339.848942950851));
#26760=CARTESIAN_POINT('Ctrl Pts',(24.0044775683968,0.958055473912675,339.825986368285));
#26761=CARTESIAN_POINT('Ctrl Pts',(23.9967304250909,1.09238764926478,339.79736320451));
#26762=CARTESIAN_POINT('Ctrl Pts',(23.9889832817851,1.22525344996556,339.763185598509));
#26763=CARTESIAN_POINT('Ctrl Pts',(23.981234396757,1.35814912171897,339.729000308658));
#26764=CARTESIAN_POINT('Ctrl Pts',(23.973485511729,1.48957738433362,339.689258189053));
#26765=CARTESIAN_POINT('Ctrl Pts',(23.9657366267009,1.61904849823985,339.644121555563));
#26766=CARTESIAN_POINT('Ctrl Pts',(23.9579795169262,1.74865703412442,339.598937013584));
#26767=CARTESIAN_POINT('Ctrl Pts',(23.9502224071514,1.87630390195221,339.548346648788));
#26768=CARTESIAN_POINT('Ctrl Pts',(23.9424652973767,2.00151784486931,339.492561560977));
#26769=CARTESIAN_POINT('Ctrl Pts',(23.9347040424505,2.12679869811386,339.436746663399));
#26770=CARTESIAN_POINT('Ctrl Pts',(23.9269427875244,2.24964368603234,339.375731685374));
#26771=CARTESIAN_POINT('Ctrl Pts',(23.9191815325982,2.3696061233979,339.309773762329));
#26772=CARTESIAN_POINT('Ctrl Pts',(23.9114078621936,2.48976046156758,339.243710328102));
#26773=CARTESIAN_POINT('Ctrl Pts',(23.9036341917889,2.60702270024926,339.172688350726));
#26774=CARTESIAN_POINT('Ctrl Pts',(23.8958605213843,2.72097436988642,339.097008852922));
#26775=CARTESIAN_POINT('Ctrl Pts',(23.8884487172072,2.82962156188694,339.024852253948));
#26776=CARTESIAN_POINT('Ctrl Pts',(23.88103691303,2.93525922944795,338.9484621601));
#26777=CARTESIAN_POINT('Ctrl Pts',(23.8736251088529,3.0375540941927,338.868132390102));
#26778=CARTESIAN_POINT('Ctrl Pts',(23.8658500300745,3.14486273497919,338.783865418786));
#26779=CARTESIAN_POINT('Ctrl Pts',(23.858074951296,3.24883172120144,338.694996516759));
#26780=CARTESIAN_POINT('Ctrl Pts',(23.8502998725176,3.34904097214365,338.601820044006));
#26781=CARTESIAN_POINT('Ctrl Pts',(23.8425343614686,3.44912690922296,338.508758230834));
#26782=CARTESIAN_POINT('Ctrl Pts',(23.8347688504196,3.54546203310141,338.411399657506));
#26783=CARTESIAN_POINT('Ctrl Pts',(23.8270033393706,3.63765738621025,338.310080331812));
#26784=CARTESIAN_POINT('Ctrl Pts',(23.8192455278484,3.72976132735801,338.208861464525));
#26785=CARTESIAN_POINT('Ctrl Pts',(23.8114877163261,3.81773340474025,338.103689947257));
#26786=CARTESIAN_POINT('Ctrl Pts',(23.8037299048039,3.90122002706017,337.994939959826));
#26787=CARTESIAN_POINT('Ctrl Pts',(23.7959779312809,3.98464382304916,337.88627181021));
#26788=CARTESIAN_POINT('Ctrl Pts',(23.788225957758,4.06358864557617,337.77403085934));
#26789=CARTESIAN_POINT('Ctrl Pts',(23.780473984235,4.13774011533684,337.658625547239));
#26790=CARTESIAN_POINT('Ctrl Pts',(23.7727252936773,4.21186018190613,337.543269109356));
#26791=CARTESIAN_POINT('Ctrl Pts',(23.7649766031197,4.28119072235909,337.424751303782));
#26792=CARTESIAN_POINT('Ctrl Pts',(23.7572279125621,4.3454599014739,337.303510648376));
#26793=CARTESIAN_POINT('Ctrl Pts',(23.7494808341843,4.40971570884922,337.182295218101));
#26794=CARTESIAN_POINT('Ctrl Pts',(23.7417337558065,4.46891206653934,337.05835840996));
#26795=CARTESIAN_POINT('Ctrl Pts',(23.7339866774286,4.52282264992869,336.932164159639));
#26796=CARTESIAN_POINT('Ctrl Pts',(23.7262395341228,4.57673368514065,336.805968851687));
#26797=CARTESIAN_POINT('Ctrl Pts',(23.718492390817,4.62535870413508,336.677516423267));
#26798=CARTESIAN_POINT('Ctrl Pts',(23.7107452475111,4.66851933469962,336.547291273173));
#26799=CARTESIAN_POINT('Ctrl Pts',(23.702996362483,4.71168966869018,336.4170368457));
#26800=CARTESIAN_POINT('Ctrl Pts',(23.6952474774549,4.74939304670637,336.285009274448));
#26801=CARTESIAN_POINT('Ctrl Pts',(23.6874985924268,4.7815009374426,336.151708230298));
#26802=CARTESIAN_POINT('Ctrl Pts',(23.6797414826521,4.81364290782583,336.018265699042));
#26803=CARTESIAN_POINT('Ctrl Pts',(23.6719843728774,4.84017743532795,335.883547375394));
#26804=CARTESIAN_POINT('Ctrl Pts',(23.6642272631027,4.86102701415203,335.74806378751));
#26805=CARTESIAN_POINT('Ctrl Pts',(23.6564660081765,4.88188773432438,335.612507801529));
#26806=CARTESIAN_POINT('Ctrl Pts',(23.6487047532503,4.89705740941223,335.476186124758));
#26807=CARTESIAN_POINT('Ctrl Pts',(23.6409434983242,4.90651054307436,335.339613535066));
#26808=CARTESIAN_POINT('Ctrl Pts',(23.6331698279195,4.91597879866959,335.20282247374));
#26809=CARTESIAN_POINT('Ctrl Pts',(23.6253961575148,4.91971222856349,335.065780088354));
#26810=CARTESIAN_POINT('Ctrl Pts',(23.6176224871101,4.91773751129472,334.929001179553));
#26811=CARTESIAN_POINT('Ctrl Pts',(23.6102106829331,4.91585471758991,334.798589361865));
#26812=CARTESIAN_POINT('Ctrl Pts',(23.6027988787561,4.90878326136743,334.668417330489));
#26813=CARTESIAN_POINT('Ctrl Pts',(23.595387074579,4.89658986500686,334.538924348494));
#26814=CARTESIAN_POINT('Ctrl Pts',(23.5876119958006,4.88379883396834,334.40308452971));
#26815=CARTESIAN_POINT('Ctrl Pts',(23.5798369170221,4.86533066250375,334.267562728932));
#26816=CARTESIAN_POINT('Ctrl Pts',(23.5720618382437,4.84120555442294,334.132871496072));
#26817=CARTESIAN_POINT('Ctrl Pts',(23.5642963271947,4.8171101338235,333.998346009349));
#26818=CARTESIAN_POINT('Ctrl Pts',(23.5565308161457,4.78737169569653,333.864649437998));
#26819=CARTESIAN_POINT('Ctrl Pts',(23.5487653050967,4.7520623089033,333.732290697833));
#26820=CARTESIAN_POINT('Ctrl Pts',(23.5410074935744,4.71678793146985,333.600063191744));
#26821=CARTESIAN_POINT('Ctrl Pts',(23.5332496820523,4.67595369777122,333.469171252337));
#26822=CARTESIAN_POINT('Ctrl Pts',(23.5254918705301,4.62968291506037,333.340114712247));
#26823=CARTESIAN_POINT('Ctrl Pts',(23.5177398970071,4.58344695258084,333.211155291297));
#26824=CARTESIAN_POINT('Ctrl Pts',(23.509987923484,4.53178271576097,333.084028886919));
#26825=CARTESIAN_POINT('Ctrl Pts',(23.502235949961,4.47486354184832,332.959220897712));
#26826=CARTESIAN_POINT('Ctrl Pts',(23.4944872594033,4.41796847323969,332.834465764762));
#26827=CARTESIAN_POINT('Ctrl Pts',(23.4867385688457,4.35582305569116,332.712027449047));
#26828=CARTESIAN_POINT('Ctrl Pts',(23.4789898782881,4.28864894258796,332.592371849778));
#26829=CARTESIAN_POINT('Ctrl Pts',(23.4712427999102,4.22148880562005,332.472741145857));
#26830=CARTESIAN_POINT('Ctrl Pts',(23.4634957215324,4.14930224541115,332.355892347399));
#26831=CARTESIAN_POINT('Ctrl Pts',(23.4557486431546,4.07235691813991,332.242266837822));
#26832=CARTESIAN_POINT('Ctrl Pts',(23.4480014998488,3.99541094599271,332.128640375953));
#26833=CARTESIAN_POINT('Ctrl Pts',(23.440254356543,3.91370634640223,332.018237580494));
#26834=CARTESIAN_POINT('Ctrl Pts',(23.4325072132372,3.82755393321118,331.911470584427));
#26835=CARTESIAN_POINT('Ctrl Pts',(23.4247583282091,3.74138215112858,331.804679584873));
#26836=CARTESIAN_POINT('Ctrl Pts',(23.417009443181,3.65076081104152,331.701526315387));
#26837=CARTESIAN_POINT('Ctrl Pts',(23.4092605581529,3.55604054119053,331.602389261274));
#26838=CARTESIAN_POINT('Ctrl Pts',(23.4015034483781,3.46121973426648,331.503146982066));
#26839=CARTESIAN_POINT('Ctrl Pts',(23.3937463386034,3.36229157720325,331.407929716738));
#26840=CARTESIAN_POINT('Ctrl Pts',(23.3859892288287,3.25964344118676,331.317078917649));
#26841=CARTESIAN_POINT('Ctrl Pts',(23.3782279739025,3.15694045328837,331.226179570797));
#26842=CARTESIAN_POINT('Ctrl Pts',(23.3704667189763,3.05051382862137,331.139651585947));
#26843=CARTESIAN_POINT('Ctrl Pts',(23.3627054640501,2.94078265734624,331.057794979361));
#26844=CARTESIAN_POINT('Ctrl Pts',(23.3549317936455,2.83087595195851,330.975807428881));
#26845=CARTESIAN_POINT('Ctrl Pts',(23.3471581232408,2.71765445955635,330.898506409812));
#26846=CARTESIAN_POINT('Ctrl Pts',(23.3393844528362,2.60156552427244,330.826148075768));
#26847=CARTESIAN_POINT('Ctrl Pts',(23.3319726486591,2.49088055685538,330.757158039582));
#26848=CARTESIAN_POINT('Ctrl Pts',(23.324560844482,2.37758934785036,330.692661022535));
#26849=CARTESIAN_POINT('Ctrl Pts',(23.3171490403049,2.26209739025036,330.632838626805));
#26850=CARTESIAN_POINT('Ctrl Pts',(23.3093739615264,2.14094482777552,330.570084157259));
#26851=CARTESIAN_POINT('Ctrl Pts',(23.301598882748,2.01698746698734,330.512275814005));
#26852=CARTESIAN_POINT('Ctrl Pts',(23.2938238039696,1.8906672554832,330.459673977395));
#26853=CARTESIAN_POINT('Ctrl Pts',(23.2860582929206,1.76450248904125,330.407136870694));
#26854=CARTESIAN_POINT('Ctrl Pts',(23.2782927818715,1.63598101463931,330.359793671491));
#26855=CARTESIAN_POINT('Ctrl Pts',(23.2705272708225,1.5055697910384,330.317859179092));
#26856=CARTESIAN_POINT('Ctrl Pts',(23.2627694593003,1.37528787054529,330.275966264864));
#26857=CARTESIAN_POINT('Ctrl Pts',(23.2550116477781,1.24312029931855,330.239471504151));
#26858=CARTESIAN_POINT('Ctrl Pts',(23.2472538362559,1.1095541259149,330.208541693371));
#26859=CARTESIAN_POINT('Ctrl Pts',(23.2395018627329,0.976088465292541,330.177635158255));
#26860=CARTESIAN_POINT('Ctrl Pts',(23.2317498892099,0.841226676692455,330.152285325285));
#26861=CARTESIAN_POINT('Ctrl Pts',(23.2239979156869,0.705470744880478,330.132609108504));
#26862=CARTESIAN_POINT('Ctrl Pts',(23.2162492251293,0.569772305786223,330.112941224613));
#26863=CARTESIAN_POINT('Ctrl Pts',(23.2085005345717,0.43318086265562,330.098942233901));
#26864=CARTESIAN_POINT('Ctrl Pts',(23.2007518440141,0.296208149440936,330.090677868106));
#26865=CARTESIAN_POINT('Ctrl Pts',(23.1930047656362,0.159263934543254,330.082415221781));
#26866=CARTESIAN_POINT('Ctrl Pts',(23.1852576872584,0.0219389972671578,
330.079884850665));
#26867=CARTESIAN_POINT('Ctrl Pts',(23.1775106088806,-0.115250649539025,
330.083100534861));
#26868=CARTESIAN_POINT('Ctrl Pts',(23.1697634655748,-0.252441446126399,
330.086316246008));
#26869=CARTESIAN_POINT('Ctrl Pts',(23.162016322269,-0.389496559215323,330.095278099361));
#26870=CARTESIAN_POINT('Ctrl Pts',(23.1542691789632,-0.525901218183885,
330.109947753734));
#26871=CARTESIAN_POINT('Ctrl Pts',(23.1465202939351,-0.662336543815736,
330.124620706156));
#26872=CARTESIAN_POINT('Ctrl Pts',(23.138771408907,-0.79812073577678,330.145003971305));
#26873=CARTESIAN_POINT('Ctrl Pts',(23.1310225238789,-0.932745772641469,
330.171007518527));
#26874=CARTESIAN_POINT('Ctrl Pts',(23.1232654141042,-1.06751370191141,330.197038666183));
#26875=CARTESIAN_POINT('Ctrl Pts',(23.1155083043294,-1.20111963398024,330.228701938163));
#26876=CARTESIAN_POINT('Ctrl Pts',(23.1077511945547,-1.33306680549895,330.265856365236));
#26877=CARTESIAN_POINT('Ctrl Pts',(23.0999899396285,-1.46508448536717,330.303030646447));
#26878=CARTESIAN_POINT('Ctrl Pts',(23.0922286847024,-1.59544126718632,330.345701808065));
#26879=CARTESIAN_POINT('Ctrl Pts',(23.0844674297762,-1.72365806714877,330.393679784247));
#26880=CARTESIAN_POINT('Ctrl Pts',(23.0766937593715,-1.85207997220541,330.441734509555));
#26881=CARTESIAN_POINT('Ctrl Pts',(23.0689200889668,-1.97835469447261,330.495112861041));
#26882=CARTESIAN_POINT('Ctrl Pts',(23.0611464185622,-2.10202474533145,330.553577276898));
#26883=CARTESIAN_POINT('Ctrl Pts',(23.0537346143851,-2.21993792556885,330.609320160132));
#26884=CARTESIAN_POINT('Ctrl Pts',(23.0463228102081,-2.33548321702727,330.669686117984));
#26885=CARTESIAN_POINT('Ctrl Pts',(23.0389110060311,-2.44828847103492,330.734432438104));
#26886=CARTESIAN_POINT('Ctrl Pts',(23.0311359272526,-2.56662264657159,330.802352168244));
#26887=CARTESIAN_POINT('Ctrl Pts',(23.0233608484742,-2.68231535629548,330.875307145868));
#26888=CARTESIAN_POINT('Ctrl Pts',(23.0155857696958,-2.79490847760867,330.953066634563));
#26889=CARTESIAN_POINT('Ctrl Pts',(23.0078202586468,-2.90736304591821,331.030730435256));
#26890=CARTESIAN_POINT('Ctrl Pts',(23.0000547475978,-3.01672529651027,331.113186763325));
#26891=CARTESIAN_POINT('Ctrl Pts',(22.9922892365487,-3.12256190188676,331.200159183415));
#26892=CARTESIAN_POINT('Ctrl Pts',(22.9845314250265,-3.22829356996095,331.287045370097));
#26893=CARTESIAN_POINT('Ctrl Pts',(22.9767736135044,-3.33050624939113,331.378438491322));
#26894=CARTESIAN_POINT('Ctrl Pts',(22.9690158019822,-3.42879610758851,331.474019240681));
#26895=CARTESIAN_POINT('Ctrl Pts',(22.9612638284591,-3.5270119995505,331.569528062496));
#26896=CARTESIAN_POINT('Ctrl Pts',(22.953511854936,-3.62131066708929,331.669217968486));
#26897=CARTESIAN_POINT('Ctrl Pts',(22.945759881413,-3.71132214193107,331.772730097852));
#26898=CARTESIAN_POINT('Ctrl Pts',(22.9380111908554,-3.80129549685981,331.876198389769));
#26899=CARTESIAN_POINT('Ctrl Pts',(22.9302625002978,-3.8869850142979,331.983485391212));
#26900=CARTESIAN_POINT('Ctrl Pts',(22.9225138097402,-3.96805849042088,332.094196345398));
#26901=CARTESIAN_POINT('Ctrl Pts',(22.9147667313624,-4.04911509853001,332.204884265245));
#26902=CARTESIAN_POINT('Ctrl Pts',(22.9070196529846,-4.12555734484776,332.318994405696));
#26903=CARTESIAN_POINT('Ctrl Pts',(22.8992725746067,-4.1970943972307,332.436100297743));
#26904=CARTESIAN_POINT('Ctrl Pts',(22.8915254313009,-4.26863204916294,332.553207171249));
#26905=CARTESIAN_POINT('Ctrl Pts',(22.8837782879951,-4.33526422139886,332.673309512869));
#26906=CARTESIAN_POINT('Ctrl Pts',(22.8760311446893,-4.39674458393906,332.795953692387));
#26907=CARTESIAN_POINT('Ctrl Pts',(22.8682822596612,-4.45823876857003,332.918625444921));
#26908=CARTESIAN_POINT('Ctrl Pts',(22.860533374633,-4.51457866361392,333.043839823133));
#26909=CARTESIAN_POINT('Ctrl Pts',(22.8527844896049,-4.565565058224,333.171120900217));
#26910=CARTESIAN_POINT('Ctrl Pts',(22.8450273798302,-4.61660557032018,333.298537074751));
#26911=CARTESIAN_POINT('Ctrl Pts',(22.8372702700555,-4.66228108555537,333.428023966692));
#26912=CARTESIAN_POINT('Ctrl Pts',(22.8295131602808,-4.70244132081064,333.559087550601));
#26913=CARTESIAN_POINT('Ctrl Pts',(22.8217519053546,-4.74262301641147,333.690221170699));
#26914=CARTESIAN_POINT('Ctrl Pts',(22.8139906504285,-4.77728346077039,333.822932783593));
#26915=CARTESIAN_POINT('Ctrl Pts',(22.8062293955024,-4.80632322457161,333.956716661954));
#26916=CARTESIAN_POINT('Ctrl Pts',(22.7984557250977,-4.83540944253091,334.090714550922));
#26917=CARTESIAN_POINT('Ctrl Pts',(22.790682054693,-4.85885694585041,334.225787747667));
#26918=CARTESIAN_POINT('Ctrl Pts',(22.7829083842883,-4.87661793197799,334.361422981927));
#26919=CARTESIAN_POINT('Ctrl Pts',(22.7754965801112,-4.89355213992822,334.4907443634));
#26920=CARTESIAN_POINT('Ctrl Pts',(22.7680847759342,-4.90531730531503,334.62057634763));
#26921=CARTESIAN_POINT('Ctrl Pts',(22.7606729717571,-4.91191613913101,334.75047464128));
#26922=CARTESIAN_POINT('Ctrl Pts',(22.7559607306682,-4.91611151384736,334.833060751504));
#26923=CARTESIAN_POINT('Ctrl Pts',(22.7512484895792,-4.91822421825937,334.915753557196));
#26924=CARTESIAN_POINT('Ctrl Pts',(22.7465362484902,-4.91824976548699,334.998481188888));
#26925=CARTESIAN_POINT('',(26.2465362485261,-4.91824994013874,334.999232650495));
#26926=CARTESIAN_POINT('Ctrl Pts',(26.2465362484902,-4.91824994013884,334.999232651133));
#26927=CARTESIAN_POINT('Ctrl Pts',(26.2385101248523,-4.91827217345382,335.141734979221));
#26928=CARTESIAN_POINT('Ctrl Pts',(26.2304840012145,-4.9120967350768,335.284149552615));
#26929=CARTESIAN_POINT('Ctrl Pts',(26.2224578775766,-4.89977251782948,335.425925270468));
#26930=CARTESIAN_POINT('Ctrl Pts',(26.2144242186472,-4.8874367300441,335.56783409384));
#26931=CARTESIAN_POINT('Ctrl Pts',(26.2063905597178,-4.86894068098241,335.709102518273));
#26932=CARTESIAN_POINT('Ctrl Pts',(26.1983569007885,-4.84438482869667,335.849187078325));
#26933=CARTESIAN_POINT('Ctrl Pts',(26.1901212743098,-4.8192116381157,335.992793387998));
#26934=CARTESIAN_POINT('Ctrl Pts',(26.1818856478311,-4.78767002512742,336.135155135803));
#26935=CARTESIAN_POINT('Ctrl Pts',(26.1736500213524,-4.74992278204833,336.275702405374));
#26936=CARTESIAN_POINT('Ctrl Pts',(26.1655921118387,-4.71299008847468,336.413216798911));
#26937=CARTESIAN_POINT('Ctrl Pts',(26.157534202325,-4.6701170328828,336.548993920819));
#26938=CARTESIAN_POINT('Ctrl Pts',(26.1494762928112,-4.62150526674811,336.682519578465));
#26939=CARTESIAN_POINT('Ctrl Pts',(26.1411518078501,-4.57128530393603,336.820462592979));
#26940=CARTESIAN_POINT('Ctrl Pts',(26.132827322889,-4.51494057631685,336.956002231368));
#26941=CARTESIAN_POINT('Ctrl Pts',(26.1245028379278,-4.45274510224256,337.088598601205));
#26942=CARTESIAN_POINT('Ctrl Pts',(26.1161783529667,-4.3905496281682,337.221194971042));
#26943=CARTESIAN_POINT('Ctrl Pts',(26.1078538680055,-4.32250365674387,337.350847748008));
#26944=CARTESIAN_POINT('Ctrl Pts',(26.0995293830443,-4.24893028952669,337.477049546788));
#26945=CARTESIAN_POINT('Ctrl Pts',(26.0917543042658,-4.18021267771288,337.594922175795));
#26946=CARTESIAN_POINT('Ctrl Pts',(26.0839792254874,-4.10647777830166,337.710119382585));
#26947=CARTESIAN_POINT('Ctrl Pts',(26.0762041467089,-4.02795941738535,337.822184613805));
#26948=CARTESIAN_POINT('Ctrl Pts',(26.0684386356599,-3.94953767831086,337.934111941623));
#26949=CARTESIAN_POINT('Ctrl Pts',(26.0606731246109,-3.86634441203466,338.042914645356));
#26950=CARTESIAN_POINT('Ctrl Pts',(26.0529076135618,-3.77865897503923,338.148161274912));
#26951=CARTESIAN_POINT('Ctrl Pts',(26.0451498020396,-3.69106047840993,338.253303552128));
#26952=CARTESIAN_POINT('Ctrl Pts',(26.0373919905174,-3.59897892336001,338.354896473452));
#26953=CARTESIAN_POINT('Ctrl Pts',(26.0296341789952,-3.50273633718802,338.452538372653));
#26954=CARTESIAN_POINT('Ctrl Pts',(26.0218822054721,-3.40656617661389,338.550106793229));
#26955=CARTESIAN_POINT('Ctrl Pts',(26.0141302319491,-3.30624149091604,338.643729832572));
#26956=CARTESIAN_POINT('Ctrl Pts',(26.006378258426,-3.20212363210602,338.733039955212));
#26957=CARTESIAN_POINT('Ctrl Pts',(25.9986295678684,-3.09804986727132,338.822312254962));
#26958=CARTESIAN_POINT('Ctrl Pts',(25.9908808773107,-2.99018642042605,338.907275016876));
#26959=CARTESIAN_POINT('Ctrl Pts',(25.9831321867531,-2.87893028361868,338.987598711576));
#26960=CARTESIAN_POINT('Ctrl Pts',(25.9753851083752,-2.7676972945798,339.06790569426));
#26961=CARTESIAN_POINT('Ctrl Pts',(25.9676380299974,-2.65307333633156,339.143575300916));
#26962=CARTESIAN_POINT('Ctrl Pts',(25.9598909516195,-2.53548683292859,339.214319587139));
#26963=CARTESIAN_POINT('Ctrl Pts',(25.9521438083137,-2.41789934403746,339.285064466268));
#26964=CARTESIAN_POINT('Ctrl Pts',(25.9443966650078,-2.29734959539829,339.350883741123));
#26965=CARTESIAN_POINT('Ctrl Pts',(25.936649521702,-2.17429287100784,339.411534151923));
#26966=CARTESIAN_POINT('Ctrl Pts',(25.9289006366739,-2.05120848085335,339.472198198223));
#26967=CARTESIAN_POINT('Ctrl Pts',(25.9211517516458,-1.92561634393892,339.52769089531));
#26968=CARTESIAN_POINT('Ctrl Pts',(25.9134028666177,-1.79799372202223,339.577816252109));
#26969=CARTESIAN_POINT('Ctrl Pts',(25.9056457568429,-1.67023564013588,339.627994812479));
#26970=CARTESIAN_POINT('Ctrl Pts',(25.8978886470682,-1.5404431324707,339.672794509247));
#26971=CARTESIAN_POINT('Ctrl Pts',(25.8901315372935,-1.40911122846013,339.712068400217));
#26972=CARTESIAN_POINT('Ctrl Pts',(25.8823702823673,-1.27770914487934,339.7513632779));
#26973=CARTESIAN_POINT('Ctrl Pts',(25.8746090274411,-1.14476640449553,339.78512636987));
#26974=CARTESIAN_POINT('Ctrl Pts',(25.8668477725149,-1.0107893948121,339.813261665631));
#26975=CARTESIAN_POINT('Ctrl Pts',(25.8590741021102,-0.876598065576192,
339.841441968696));
#26976=CARTESIAN_POINT('Ctrl Pts',(25.8513004317056,-0.741369546632563,
339.863976421327));
#26977=CARTESIAN_POINT('Ctrl Pts',(25.8435267613009,-0.605617419472553,
339.88082068957));
#26978=CARTESIAN_POINT('Ctrl Pts',(25.8361149571241,-0.476184586497428,
339.896880853072));
#26979=CARTESIAN_POINT('Ctrl Pts',(25.8287031529473,-0.346276082980034,
339.907768642485));
#26980=CARTESIAN_POINT('Ctrl Pts',(25.8212913487705,-0.216336173803566,
339.913489770255));
#26981=CARTESIAN_POINT('Ctrl Pts',(25.813516269992,-0.0800275226018157,
339.919491307541));
#26982=CARTESIAN_POINT('Ctrl Pts',(25.8057411912136,0.0567464511916358,
339.919825876169));
#26983=CARTESIAN_POINT('Ctrl Pts',(25.7979661124351,0.193475285405127,339.914443038274));
#26984=CARTESIAN_POINT('Ctrl Pts',(25.7902006013861,0.330035866083349,339.909066824303));
#26985=CARTESIAN_POINT('Ctrl Pts',(25.7824350903372,0.466551030866433,339.897987217929));
#26986=CARTESIAN_POINT('Ctrl Pts',(25.7746695792882,0.6025067883454,339.881205653576));
#26987=CARTESIAN_POINT('Ctrl Pts',(25.766911767766,0.738327745295094,339.864440728192));
#26988=CARTESIAN_POINT('Ctrl Pts',(25.7591539562437,0.873590013302157,339.841985143206));
#26989=CARTESIAN_POINT('Ctrl Pts',(25.7513961447216,1.00778155521446,339.813892333598));
#26990=CARTESIAN_POINT('Ctrl Pts',(25.7436441711986,1.14187211373546,339.785820664719));
#26991=CARTESIAN_POINT('Ctrl Pts',(25.7358921976756,1.27489316893825,339.75212029486));
#26992=CARTESIAN_POINT('Ctrl Pts',(25.7281402241526,1.4063401040965,339.712896198105));
#26993=CARTESIAN_POINT('Ctrl Pts',(25.720391533595,1.53773137140039,339.673688712777));
#26994=CARTESIAN_POINT('Ctrl Pts',(25.7126428430373,1.66754947078681,339.628962264794));
#26995=CARTESIAN_POINT('Ctrl Pts',(25.7048941524797,1.79530245879277,339.578872365982));
#26996=CARTESIAN_POINT('Ctrl Pts',(25.6971470741018,1.92302886672238,339.528792888792));
#26997=CARTESIAN_POINT('Ctrl Pts',(25.689399995724,2.04869065422893,339.473352322989));
#26998=CARTESIAN_POINT('Ctrl Pts',(25.6816529173462,2.17181383788041,339.412755116261));
#26999=CARTESIAN_POINT('Ctrl Pts',(25.6739057740404,2.29493805342277,339.352157401671));
#27000=CARTESIAN_POINT('Ctrl Pts',(25.6661586307346,2.41552327197314,339.286403132558));
#27001=CARTESIAN_POINT('Ctrl Pts',(25.6584114874287,2.5331185508954,339.215743525122));
#27002=CARTESIAN_POINT('Ctrl Pts',(25.6506626024006,2.65074026773281,339.145068031906));
#27003=CARTESIAN_POINT('Ctrl Pts',(25.6429137173726,2.7653703723578,339.069485207149));
#27004=CARTESIAN_POINT('Ctrl Pts',(25.6351648323445,2.87658577797066,338.989290328426));
#27005=CARTESIAN_POINT('Ctrl Pts',(25.6274077225698,2.98791922876426,338.909010330031));
#27006=CARTESIAN_POINT('Ctrl Pts',(25.619650612795,3.0958304229264,338.824108727861));
#27007=CARTESIAN_POINT('Ctrl Pts',(25.6118935030203,3.19992790479848,338.734922283876));
#27008=CARTESIAN_POINT('Ctrl Pts',(25.6041322480941,3.30408101303641,338.645688181506));
#27009=CARTESIAN_POINT('Ctrl Pts',(25.5963709931679,3.40441606245316,338.5521649413));
#27010=CARTESIAN_POINT('Ctrl Pts',(25.5886097382418,3.50057828043755,338.454726438523));
#27011=CARTESIAN_POINT('Ctrl Pts',(25.5808360678371,3.59689432663153,338.357132065896));
#27012=CARTESIAN_POINT('Ctrl Pts',(25.5730623974324,3.68902393961181,338.255610204689));
#27013=CARTESIAN_POINT('Ctrl Pts',(25.5652887270277,3.7766519095954,338.150568744886));
#27014=CARTESIAN_POINT('Ctrl Pts',(25.5578769228506,3.86020077649395,338.050416990308));
#27015=CARTESIAN_POINT('Ctrl Pts',(25.5504651186736,3.93965749629635,337.947066165813));
#27016=CARTESIAN_POINT('Ctrl Pts',(25.5430533144965,4.01478645550223,337.840892954551));
#27017=CARTESIAN_POINT('Ctrl Pts',(25.5352782357181,4.09359770879637,337.729515877931));
#27018=CARTESIAN_POINT('Ctrl Pts',(25.5275031569397,4.16789530000232,337.614680779707));
#27019=CARTESIAN_POINT('Ctrl Pts',(25.5197280781613,4.23736057446958,337.496789623583));
#27020=CARTESIAN_POINT('Ctrl Pts',(25.5119625671123,4.30674036749434,337.379043540032));
#27021=CARTESIAN_POINT('Ctrl Pts',(25.5041970560633,4.37129947902379,337.258249214786));
#27022=CARTESIAN_POINT('Ctrl Pts',(25.4964315450143,4.43076096505197,337.134839650436));
#27023=CARTESIAN_POINT('Ctrl Pts',(25.4886737334922,4.49016349484335,337.011552447028));
#27024=CARTESIAN_POINT('Ctrl Pts',(25.4809159219701,4.54447828892536,336.885655514631));
#27025=CARTESIAN_POINT('Ctrl Pts',(25.4731581104479,4.59347318922914,336.757608352942));
#27026=CARTESIAN_POINT('Ctrl Pts',(25.465406136925,4.64243121931652,336.629657550804));
#27027=CARTESIAN_POINT('Ctrl Pts',(25.457654163402,4.68607718505317,336.499560103748));
#27028=CARTESIAN_POINT('Ctrl Pts',(25.4499021898791,4.72422628431963,336.367797162244));
#27029=CARTESIAN_POINT('Ctrl Pts',(25.4421534993215,4.76235922742016,336.236090022424));
#27030=CARTESIAN_POINT('Ctrl Pts',(25.4344048087639,4.7949998256532,336.102719165696));
#27031=CARTESIAN_POINT('Ctrl Pts',(25.4266561182063,4.82201263339612,335.968182434187));
#27032=CARTESIAN_POINT('Ctrl Pts',(25.4189090398285,4.84901982089877,335.833673694169));
#27033=CARTESIAN_POINT('Ctrl Pts',(25.4111619614507,4.87040147003448,335.697999944844));
#27034=CARTESIAN_POINT('Ctrl Pts',(25.4034148830729,4.88607300559344,335.561670407366));
#27035=CARTESIAN_POINT('Ctrl Pts',(25.3956677397672,4.90174467249491,335.425339727317));
#27036=CARTESIAN_POINT('Ctrl Pts',(25.3879205964614,4.91170608572846,335.28835363647));
#27037=CARTESIAN_POINT('Ctrl Pts',(25.3801734531556,4.91592446741988,335.151227289609));
#27038=CARTESIAN_POINT('Ctrl Pts',(25.3724245681275,4.92014379749311,335.014070113833));
#27039=CARTESIAN_POINT('Ctrl Pts',(25.3646756830994,4.91861751475273,334.876773009909));
#27040=CARTESIAN_POINT('Ctrl Pts',(25.3569267980712,4.91136496786835,334.739851552195));
#27041=CARTESIAN_POINT('Ctrl Pts',(25.3491696882965,4.90410472305581,334.602784764631));
#27042=CARTESIAN_POINT('Ctrl Pts',(25.3414125785218,4.89110609359985,334.466094810689));
#27043=CARTESIAN_POINT('Ctrl Pts',(25.3336554687471,4.87244043069669,334.330293115003));
#27044=CARTESIAN_POINT('Ctrl Pts',(25.325894213821,4.85376479346011,334.194418851233));
#27045=CARTESIAN_POINT('Ctrl Pts',(25.3181329588949,4.82941615800395,334.059434175987));
#27046=CARTESIAN_POINT('Ctrl Pts',(25.3103717039687,4.79951693619806,333.92583975048));
#27047=CARTESIAN_POINT('Ctrl Pts',(25.3025980335641,4.76956988538138,333.792031617431));
#27048=CARTESIAN_POINT('Ctrl Pts',(25.2948243631595,4.73405460639817,333.659618555955));
#27049=CARTESIAN_POINT('Ctrl Pts',(25.2870506927548,4.69314352453913,333.529086365358));
#27050=CARTESIAN_POINT('Ctrl Pts',(25.2796388885774,4.65413686338139,333.404630479631));
#27051=CARTESIAN_POINT('Ctrl Pts',(25.2722270844,4.6102255404787,333.281884567405));
#27052=CARTESIAN_POINT('Ctrl Pts',(25.2648152802226,4.56159881274524,333.161250605966));
#27053=CARTESIAN_POINT('Ctrl Pts',(25.2570402014441,4.51058874423609,333.034704014731));
#27054=CARTESIAN_POINT('Ctrl Pts',(25.2492651226656,4.45422815003558,332.91008172433));
#27055=CARTESIAN_POINT('Ctrl Pts',(25.2414900438872,4.39268260768378,332.787869223881));
#27056=CARTESIAN_POINT('Ctrl Pts',(25.2337245328381,4.3312128010402,332.665807113695));
#27057=CARTESIAN_POINT('Ctrl Pts',(25.2259590217891,4.26457091555621,332.546149238934));
#27058=CARTESIAN_POINT('Ctrl Pts',(25.2181935107401,4.19297120205544,332.429362810268));
#27059=CARTESIAN_POINT('Ctrl Pts',(25.2104356992179,4.12144247987893,332.312692175686));
#27060=CARTESIAN_POINT('Ctrl Pts',(25.2026778876957,4.04496591519182,332.198887652501));
#27061=CARTESIAN_POINT('Ctrl Pts',(25.1949200761734,3.96380227704169,332.08839312904));
#27062=CARTESIAN_POINT('Ctrl Pts',(25.1871681026504,3.88269971710344,331.977981756213));
#27063=CARTESIAN_POINT('Ctrl Pts',(25.1794161291274,3.79691733483057,331.870875738886));
#27064=CARTESIAN_POINT('Ctrl Pts',(25.1716641556044,3.70675973288782,331.767490859233));
#27065=CARTESIAN_POINT('Ctrl Pts',(25.1639154650468,3.61664031274264,331.664149763138));
#27066=CARTESIAN_POINT('Ctrl Pts',(25.1561667744891,3.52214961459789,331.564526964333));
#27067=CARTESIAN_POINT('Ctrl Pts',(25.1484180839315,3.42363298712003,331.469005772873));
#27068=CARTESIAN_POINT('Ctrl Pts',(25.1406710055536,3.32513685684934,331.373504455395));
#27069=CARTESIAN_POINT('Ctrl Pts',(25.1329239271758,3.22261674379429,331.282103319761));
#27070=CARTESIAN_POINT('Ctrl Pts',(25.1251768487979,3.11645509438899,331.195149055856));
#27071=CARTESIAN_POINT('Ctrl Pts',(25.1174297054921,3.01029255524667,331.10819406319));
#27072=CARTESIAN_POINT('Ctrl Pts',(25.1096825621862,2.90048872126823,331.025686264266));
#27073=CARTESIAN_POINT('Ctrl Pts',(25.1019354188804,2.78745905911271,330.947932002511));
#27074=CARTESIAN_POINT('Ctrl Pts',(25.0941865338523,2.67440398548992,330.870160259948));
#27075=CARTESIAN_POINT('Ctrl Pts',(25.0864376488242,2.55812196252632,330.797144402628));
#27076=CARTESIAN_POINT('Ctrl Pts',(25.0786887637961,2.43905701837231,330.729147166709));
#27077=CARTESIAN_POINT('Ctrl Pts',(25.0709316540213,2.31986569745623,330.661077757821));
#27078=CARTESIAN_POINT('Ctrl Pts',(25.0631745442466,2.19788589477356,330.598037805299));
#27079=CARTESIAN_POINT('Ctrl Pts',(25.0554174344718,2.07358629043573,330.540244069614));
#27080=CARTESIAN_POINT('Ctrl Pts',(25.0476561795456,1.94922026436376,330.482419450804));
#27081=CARTESIAN_POINT('Ctrl Pts',(25.0398949246194,1.82253232740655,330.42984678462));
#27082=CARTESIAN_POINT('Ctrl Pts',(25.0321336696933,1.69400974034882,330.382694068821));
#27083=CARTESIAN_POINT('Ctrl Pts',(25.0243599992886,1.56528155903705,330.335465924043));
#27084=CARTESIAN_POINT('Ctrl Pts',(25.0165863288839,1.43471323540737,330.293675174401));
#27085=CARTESIAN_POINT('Ctrl Pts',(25.0088126584792,1.30280659767993,330.257439717669));
#27086=CARTESIAN_POINT('Ctrl Pts',(25.0014008543023,1.17704024567806,330.222891030167));
#27087=CARTESIAN_POINT('Ctrl Pts',(24.9939890501255,1.05005765297368,330.193392142141));
#27088=CARTESIAN_POINT('Ctrl Pts',(24.9865772459486,0.922299268618735,330.16900143639));
#27089=CARTESIAN_POINT('Ctrl Pts',(24.9788021671702,0.788279065269675,330.143415269492));
#27090=CARTESIAN_POINT('Ctrl Pts',(24.9710270883917,0.652981571079474,330.123369823394));
#27091=CARTESIAN_POINT('Ctrl Pts',(24.9632520096133,0.516904647714207,330.10898858643));
#27092=CARTESIAN_POINT('Ctrl Pts',(24.9554864985643,0.380995175665853,330.094625046493));
#27093=CARTESIAN_POINT('Ctrl Pts',(24.9477209875153,0.244308567844098,330.085911887738));
#27094=CARTESIAN_POINT('Ctrl Pts',(24.9399554764662,0.107353655083676,330.082921776579));
#27095=CARTESIAN_POINT('Ctrl Pts',(24.932197664944,-0.0294654664817331,
330.079934630124));
#27096=CARTESIAN_POINT('Ctrl Pts',(24.9244398534218,-0.1665519753169,330.082659247328));
#27097=CARTESIAN_POINT('Ctrl Pts',(24.9166820418996,-0.303391479163863,
330.091116555379));
#27098=CARTESIAN_POINT('Ctrl Pts',(24.9089300683766,-0.440128006944566,
330.099567499038));
#27099=CARTESIAN_POINT('Ctrl Pts',(24.9011780948535,-0.576617511161267,
330.113742522661));
#27100=CARTESIAN_POINT('Ctrl Pts',(24.8934261213305,-0.712345513734498,
330.133610482959));
#27101=CARTESIAN_POINT('Ctrl Pts',(24.8856774307729,-0.848016035417872,
330.153470029165));
#27102=CARTESIAN_POINT('Ctrl Pts',(24.8779287402153,-0.982925310932581,
330.179017660317));
#27103=CARTESIAN_POINT('Ctrl Pts',(24.8701800496577,-1.11656411869695,330.210170396419));
#27104=CARTESIAN_POINT('Ctrl Pts',(24.8624329712799,-1.25017512179138,330.241316650935));
#27105=CARTESIAN_POINT('Ctrl Pts',(24.854685892902,-1.38251580248019,330.278065602085));
#27106=CARTESIAN_POINT('Ctrl Pts',(24.8469388145242,-1.51308765813306,330.320283256296));
#27107=CARTESIAN_POINT('Ctrl Pts',(24.8391916712183,-1.64366060810384,330.362501264331));
#27108=CARTESIAN_POINT('Ctrl Pts',(24.8314445279125,-1.77246433155314,330.410187946591));
#27109=CARTESIAN_POINT('Ctrl Pts',(24.8236973846067,-1.89901638490937,330.463159708305));
#27110=CARTESIAN_POINT('Ctrl Pts',(24.8159484995787,-2.02559688985346,330.516143379196));
#27111=CARTESIAN_POINT('Ctrl Pts',(24.8081996145506,-2.14992435688523,330.574414343029));
#27112=CARTESIAN_POINT('Ctrl Pts',(24.8004507295225,-2.27153755645328,330.63774138867));
#27113=CARTESIAN_POINT('Ctrl Pts',(24.7926936197478,-2.39327983752818,330.701135650292));
#27114=CARTESIAN_POINT('Ctrl Pts',(24.784936509973,-2.51230174893353,330.769596533151));
#27115=CARTESIAN_POINT('Ctrl Pts',(24.7771794001983,-2.62816738246323,330.842847215671));
#27116=CARTESIAN_POINT('Ctrl Pts',(24.7694181452721,-2.74409493088274,330.916137041013));
#27117=CARTESIAN_POINT('Ctrl Pts',(24.761656890346,-2.85686251950509,330.994221543677));
#27118=CARTESIAN_POINT('Ctrl Pts',(24.7538956354198,-2.96606519066085,331.076781888902));
#27119=CARTESIAN_POINT('Ctrl Pts',(24.7461219650152,-3.07544255050139,331.159474303772));
#27120=CARTESIAN_POINT('Ctrl Pts',(24.7383482946105,-3.18124329536648,331.24665662008));
#27121=CARTESIAN_POINT('Ctrl Pts',(24.7305746242059,-3.28309671445723,331.337970641022));
#27122=CARTESIAN_POINT('Ctrl Pts',(24.7231628200288,-3.38020883238479,331.425033972319));
#27123=CARTESIAN_POINT('Ctrl Pts',(24.7157510158517,-3.47373264383196,331.515852802625));
#27124=CARTESIAN_POINT('Ctrl Pts',(24.7083392116747,-3.56338070120289,331.610088343217));
#27125=CARTESIAN_POINT('Ctrl Pts',(24.7006598905743,-3.65626445826493,331.707725161187));
#27126=CARTESIAN_POINT('Ctrl Pts',(24.6929805694739,-3.74529721302402,331.809355905759));
#27127=CARTESIAN_POINT('Ctrl Pts',(24.6853012483735,-3.83010939108351,331.91464019686));
#27128=CARTESIAN_POINT('Ctrl Pts',(24.6774360400451,-3.91697455019225,332.022473021194));
#27129=CARTESIAN_POINT('Ctrl Pts',(24.6695708317166,-3.99941184335112,332.134138294801));
#27130=CARTESIAN_POINT('Ctrl Pts',(24.6617056233881,-4.07706247657,332.249228358325));
#27131=CARTESIAN_POINT('Ctrl Pts',(24.6540451701267,-4.15269162988034,332.361322280781));
#27132=CARTESIAN_POINT('Ctrl Pts',(24.6463847168653,-4.22377999456111,332.476664540659));
#27133=CARTESIAN_POINT('Ctrl Pts',(24.6387242636039,-4.29003585261921,332.594843987235));
#27134=CARTESIAN_POINT('Ctrl Pts',(24.631068819397,-4.35624838697368,332.712946158057));
#27135=CARTESIAN_POINT('Ctrl Pts',(24.6234133751902,-4.4176345026729,332.833881477813));
#27136=CARTESIAN_POINT('Ctrl Pts',(24.6157579309833,-4.47394605442155,332.957210298483));
#27137=CARTESIAN_POINT('Ctrl Pts',(24.6081057372702,-4.53023369634304,333.080486753861));
#27138=CARTESIAN_POINT('Ctrl Pts',(24.600453543557,-4.58145089398798,333.206154324079));
#27139=CARTESIAN_POINT('Ctrl Pts',(24.5928013498439,-4.62739593893171,333.333749752631));
#27140=CARTESIAN_POINT('Ctrl Pts',(24.5847792580644,-4.67556191344435,333.467512994501));
#27141=CARTESIAN_POINT('Ctrl Pts',(24.576757166285,-4.71793310317526,333.603394707546));
#27142=CARTESIAN_POINT('Ctrl Pts',(24.5687350745055,-4.7543345560173,333.740839171527));
#27143=CARTESIAN_POINT('Ctrl Pts',(24.5610819356911,-4.78906182906563,333.871962273959));
#27144=CARTESIAN_POINT('Ctrl Pts',(24.5534287968767,-4.81835617095714,334.00450716053));
#27145=CARTESIAN_POINT('Ctrl Pts',(24.5457756580624,-4.84211746075958,334.137978214482));
#27146=CARTESIAN_POINT('Ctrl Pts',(24.5381208996189,-4.86588377914909,334.271477514831));
#27147=CARTESIAN_POINT('Ctrl Pts',(24.5304661411755,-4.88411465462634,334.405902975934));
#27148=CARTESIAN_POINT('Ctrl Pts',(24.5228113827321,-4.89676160564217,334.540751875335));
#27149=CARTESIAN_POINT('Ctrl Pts',(24.5151509942951,-4.90941785835635,334.67569995467));
#27150=CARTESIAN_POINT('Ctrl Pts',(24.507490605858,-4.91648196677551,334.811071693648));
#27151=CARTESIAN_POINT('Ctrl Pts',(24.499830217421,-4.91795751081103,334.94636247249));
#27152=CARTESIAN_POINT('Ctrl Pts',(24.4987322277773,-4.9181690055783,334.965754161993));
#27153=CARTESIAN_POINT('Ctrl Pts',(24.4976342381337,-4.91826577356416,334.985144192857));
#27154=CARTESIAN_POINT('Ctrl Pts',(24.4965362484901,-4.91824791280043,335.004531085324));
#27155=CARTESIAN_POINT('',(27.9965362484484,-4.91824819040164,334.995780982225));
#27156=CARTESIAN_POINT('Ctrl Pts',(27.9965362484484,-4.91824819040164,334.995780982225));
#27157=CARTESIAN_POINT('Ctrl Pts',(27.9888887221241,-4.91836378679145,335.130535506929));
#27158=CARTESIAN_POINT('Ctrl Pts',(27.9812411957999,-4.91293703731669,335.265481117084));
#27159=CARTESIAN_POINT('Ctrl Pts',(27.9735936694756,-4.90194754509121,335.400116642586));
#27160=CARTESIAN_POINT('Ctrl Pts',(27.965953003735,-4.89096791152174,335.534631386772));
#27161=CARTESIAN_POINT('Ctrl Pts',(27.9583123379943,-4.87443549378492,335.668836199799));
#27162=CARTESIAN_POINT('Ctrl Pts',(27.9506716722537,-4.8523819494007,335.802229692563));
#27163=CARTESIAN_POINT('Ctrl Pts',(27.9430355614214,-4.83034155202144,335.935543664101));
#27164=CARTESIAN_POINT('Ctrl Pts',(27.9353994505891,-4.80278663931256,336.068046880407));
#27165=CARTESIAN_POINT('Ctrl Pts',(27.9277633397567,-4.76980067974941,336.199243318915));
#27166=CARTESIAN_POINT('Ctrl Pts',(27.920129584571,-4.7368248959507,336.330399284929));
#27167=CARTESIAN_POINT('Ctrl Pts',(27.9124958293852,-4.69842149401602,336.460248883604));
#27168=CARTESIAN_POINT('Ctrl Pts',(27.9048620741995,-4.65472490221656,336.588307006591));
#27169=CARTESIAN_POINT('Ctrl Pts',(27.8972289078239,-4.61103168084217,336.716355252141));
#27170=CARTESIAN_POINT('Ctrl Pts',(27.8895957414484,-4.5620462117725,336.842611914903));
#27171=CARTESIAN_POINT('Ctrl Pts',(27.8819625750729,-4.50795240032874,336.966608303367));
#27172=CARTESIAN_POINT('Ctrl Pts',(27.8743282313581,-4.45385024545755,337.090623817029));
#27173=CARTESIAN_POINT('Ctrl Pts',(27.8666938876433,-4.39463834331634,337.212377993544));
#27174=CARTESIAN_POINT('Ctrl Pts',(27.8590595439285,-4.33054798471872,337.331423859908));
#27175=CARTESIAN_POINT('Ctrl Pts',(27.8514176237407,-4.26639402158833,337.450587869732));
#27176=CARTESIAN_POINT('Ctrl Pts',(27.8437757035531,-4.19735212412781,337.567037845476));
#27177=CARTESIAN_POINT('Ctrl Pts',(27.8361337833653,-4.12369881076348,337.68035280898));
#27178=CARTESIAN_POINT('Ctrl Pts',(27.8284880555331,-4.05000879907859,337.793724232523));
#27179=CARTESIAN_POINT('Ctrl Pts',(27.8208423277008,-3.97170303010984,337.903957204971));
#27180=CARTESIAN_POINT('Ctrl Pts',(27.8131965998685,-3.88909949679421,338.010662413246));
#27181=CARTESIAN_POINT('Ctrl Pts',(27.8055388590461,-3.80636617656312,338.11753527706));
#27182=CARTESIAN_POINT('Ctrl Pts',(27.7978811182238,-3.71932186260039,338.220868995746));
#27183=CARTESIAN_POINT('Ctrl Pts',(27.7902233774014,-3.62832316736817,338.320309331318));
#27184=CARTESIAN_POINT('Ctrl Pts',(27.7831347811636,-3.54408774812037,338.412358984731));
#27185=CARTESIAN_POINT('Ctrl Pts',(27.7760461849258,-3.45646448831866,338.501072716874));
#27186=CARTESIAN_POINT('Ctrl Pts',(27.768957588688,-3.36576112501035,338.586200651368));
#27187=CARTESIAN_POINT('Ctrl Pts',(27.7611825099096,-3.26627375522161,338.679572649819));
#27188=CARTESIAN_POINT('Ctrl Pts',(27.7534074311311,-3.16274078260526,338.768949131203));
#27189=CARTESIAN_POINT('Ctrl Pts',(27.7456323523527,-3.05551655667957,338.853959215451));
#27190=CARTESIAN_POINT('Ctrl Pts',(27.7378668413037,-2.94842427699026,338.938864689378));
#27191=CARTESIAN_POINT('Ctrl Pts',(27.7301013302547,-2.83765008527288,339.019414216642));
#27192=CARTESIAN_POINT('Ctrl Pts',(27.7223358192057,-2.7235848084545,339.095273965641));
#27193=CARTESIAN_POINT('Ctrl Pts',(27.7145780076835,-2.60963262769011,339.171058499478));
#27194=CARTESIAN_POINT('Ctrl Pts',(27.7068201961612,-2.4923961789912,339.24216229361));
#27195=CARTESIAN_POINT('Ctrl Pts',(27.699062384639,-2.37229869072276,339.308292235271));
#27196=CARTESIAN_POINT('Ctrl Pts',(27.691310411116,-2.25229157962292,339.374372412054));
#27197=CARTESIAN_POINT('Ctrl Pts',(27.6835584375931,-2.12942805546029,339.435485998811));
#27198=CARTESIAN_POINT('Ctrl Pts',(27.6758064640701,-2.00415930094692,339.491383813362));
#27199=CARTESIAN_POINT('Ctrl Pts',(27.6680577735124,-1.87894359782546,339.547257955155));
#27200=CARTESIAN_POINT('Ctrl Pts',(27.6603090829548,-1.75132504651622,339.597920559106));
#27201=CARTESIAN_POINT('Ctrl Pts',(27.6525603923972,-1.62177814700563,339.64316903681));
#27202=CARTESIAN_POINT('Ctrl Pts',(27.6448133140194,-1.49225820080949,339.688408100191));
#27203=CARTESIAN_POINT('Ctrl Pts',(27.6370662356415,-1.36081107322572,339.728235149112));
#27204=CARTESIAN_POINT('Ctrl Pts',(27.6293191572637,-1.22792952739986,339.762496418711));
#27205=CARTESIAN_POINT('Ctrl Pts',(27.6215720139579,-1.09504686789866,339.796757975453));
#27206=CARTESIAN_POINT('Ctrl Pts',(27.6138248706521,-0.960730144672856,
339.825453562243));
#27207=CARTESIAN_POINT('Ctrl Pts',(27.6060777273463,-0.82548511771542,339.848479904355));
#27208=CARTESIAN_POINT('Ctrl Pts',(27.5983288423182,-0.69020968480459,339.871511423277));
#27209=CARTESIAN_POINT('Ctrl Pts',(27.5905799572901,-0.554005918121751,
339.888871095683));
#27210=CARTESIAN_POINT('Ctrl Pts',(27.582831072262,-0.417387158036611,339.900507220973));
#27211=CARTESIAN_POINT('Ctrl Pts',(27.5750739624873,-0.280623389387794,
339.912155696966));
#27212=CARTESIAN_POINT('Ctrl Pts',(27.5673168527125,-0.143444137519326,
339.918068457172));
#27213=CARTESIAN_POINT('Ctrl Pts',(27.5595597429378,-0.00636578020518247,
339.918245880326));
#27214=CARTESIAN_POINT('Ctrl Pts',(27.5517984880116,0.1307858274001,339.918423398289));
#27215=CARTESIAN_POINT('Ctrl Pts',(27.5440372330855,0.267836042666445,339.912859488194));
#27216=CARTESIAN_POINT('Ctrl Pts',(27.5362759781593,0.40427213079559,339.90160658425));
#27217=CARTESIAN_POINT('Ctrl Pts',(27.5285023077547,0.540926472201139,339.890335679327));
#27218=CARTESIAN_POINT('Ctrl Pts',(27.52072863735,0.67696433526753,339.87335764342));
#27219=CARTESIAN_POINT('Ctrl Pts',(27.5129549669454,0.811880831709009,339.850776492233));
#27220=CARTESIAN_POINT('Ctrl Pts',(27.5055431627682,0.940516932782646,339.829246499067));
#27221=CARTESIAN_POINT('Ctrl Pts',(27.4981313585911,1.06813343529362,339.80262336002));
#27222=CARTESIAN_POINT('Ctrl Pts',(27.490719554414,1.19430616389448,339.771039283991));
#27223=CARTESIAN_POINT('Ctrl Pts',(27.4829444756356,1.32666299377277,339.737907178312));
#27224=CARTESIAN_POINT('Ctrl Pts',(27.4751693968572,1.45784921593568,339.699210835358));
#27225=CARTESIAN_POINT('Ctrl Pts',(27.4673943180787,1.58736119056331,339.655047530713));
#27226=CARTESIAN_POINT('Ctrl Pts',(27.4596288070297,1.71671379246137,339.610938571825));
#27227=CARTESIAN_POINT('Ctrl Pts',(27.4518632959807,1.84439587974724,339.56137616188));
#27228=CARTESIAN_POINT('Ctrl Pts',(27.4440977849317,1.96991522742806,339.506508300142));
#27229=CARTESIAN_POINT('Ctrl Pts',(27.4363399734095,2.09531012230978,339.451694840049));
#27230=CARTESIAN_POINT('Ctrl Pts',(27.4285821618873,2.21854618914502,339.391586552147));
#27231=CARTESIAN_POINT('Ctrl Pts',(27.4208243503651,2.33914791000277,339.326380718063));
#27232=CARTESIAN_POINT('Ctrl Pts',(27.4130723768421,2.45965887424075,339.261223953437));
#27233=CARTESIAN_POINT('Ctrl Pts',(27.4053204033192,2.57753909597758,339.190977463282));
#27234=CARTESIAN_POINT('Ctrl Pts',(27.3975684297962,2.6923348717475,339.115885809989));
#27235=CARTESIAN_POINT('Ctrl Pts',(27.3898197392386,2.80708203143853,339.040825958057));
#27236=CARTESIAN_POINT('Ctrl Pts',(27.3820710486809,2.91874701680486,338.960925237656));
#27237=CARTESIAN_POINT('Ctrl Pts',(27.3743223581233,3.02690268776494,338.876473033738));
#27238=CARTESIAN_POINT('Ctrl Pts',(27.3665752797455,3.13503585603434,338.792038400807));
#27239=CARTESIAN_POINT('Ctrl Pts',(27.3588282013677,3.23966085431551,338.703054408368));
#27240=CARTESIAN_POINT('Ctrl Pts',(27.3510811229899,3.3403817160414,338.609852220471));
#27241=CARTESIAN_POINT('Ctrl Pts',(27.3433339796841,3.44110342190513,338.516649251449));
#27242=CARTESIAN_POINT('Ctrl Pts',(27.3355868363783,3.53792063905991,338.419228281932));
#27243=CARTESIAN_POINT('Ctrl Pts',(27.3278396930725,3.63047282583165,338.317958728405));
#27244=CARTESIAN_POINT('Ctrl Pts',(27.3200908080444,3.72304582030016,338.216666407332));
#27245=CARTESIAN_POINT('Ctrl Pts',(27.3123419230162,3.81135161270188,338.111524068985));
#27246=CARTESIAN_POINT('Ctrl Pts',(27.3045930379881,3.89506892896896,338.002935414071));
#27247=CARTESIAN_POINT('Ctrl Pts',(27.2968359282134,3.97887510366026,337.894231502037));
#27248=CARTESIAN_POINT('Ctrl Pts',(27.2890788184387,4.0580828343907,337.782074276371));
#27249=CARTESIAN_POINT('Ctrl Pts',(27.281321708664,4.13241299800268,337.666898175116));
#27250=CARTESIAN_POINT('Ctrl Pts',(27.2735604537378,4.20678288127733,337.551660527436));
#27251=CARTESIAN_POINT('Ctrl Pts',(27.2657991988117,4.27626980599831,337.433401126571));
#27252=CARTESIAN_POINT('Ctrl Pts',(27.2580379438855,4.340640394989,337.312579517312));
#27253=CARTESIAN_POINT('Ctrl Pts',(27.2502642734809,4.40511395594383,337.191564632853));
#27254=CARTESIAN_POINT('Ctrl Pts',(27.2424906030762,4.46445465689536,337.067979702131));
#27255=CARTESIAN_POINT('Ctrl Pts',(27.2347169326716,4.51847674284651,336.942305585343));
#27256=CARTESIAN_POINT('Ctrl Pts',(27.2273051284944,4.56998408770003,336.822481628926));
#27257=CARTESIAN_POINT('Ctrl Pts',(27.2198933243173,4.6166567342375,336.700758881212));
#27258=CARTESIAN_POINT('Ctrl Pts',(27.2124815201402,4.65837631412361,336.577565586121));
#27259=CARTESIAN_POINT('Ctrl Pts',(27.2047064413617,4.70214069489594,336.448334220664));
#27260=CARTESIAN_POINT('Ctrl Pts',(27.1969313625833,4.74059250683218,336.317076116144));
#27261=CARTESIAN_POINT('Ctrl Pts',(27.1891562838048,4.77354100263976,336.184267435429));
#27262=CARTESIAN_POINT('Ctrl Pts',(27.1813907727558,4.80644895322569,336.05162218425));
#27263=CARTESIAN_POINT('Ctrl Pts',(27.1736252617068,4.83386696916201,335.917430529162));
#27264=CARTESIAN_POINT('Ctrl Pts',(27.1658597506578,4.85565313500078,335.782186483556));
#27265=CARTESIAN_POINT('Ctrl Pts',(27.1581019391356,4.87741769979264,335.647076532815));
#27266=CARTESIAN_POINT('Ctrl Pts',(27.1503441276133,4.89356146519102,335.51091665149));
#27267=CARTESIAN_POINT('Ctrl Pts',(27.1425863160911,4.90399299948555,335.374213473163));
#27268=CARTESIAN_POINT('Ctrl Pts',(27.1348343425681,4.91441668371969,335.237613168313));
#27269=CARTESIAN_POINT('Ctrl Pts',(27.1270823690452,4.91913666345235,335.100470768424));
#27270=CARTESIAN_POINT('Ctrl Pts',(27.1193303955222,4.91811307143793,334.963300149164));
#27271=CARTESIAN_POINT('Ctrl Pts',(27.1115817049646,4.91708991291533,334.826187621742));
#27272=CARTESIAN_POINT('Ctrl Pts',(27.1038330144069,4.91032802344049,334.689047288768));
#27273=CARTESIAN_POINT('Ctrl Pts',(27.0960843238493,4.89783960298501,334.552394944251));
#27274=CARTESIAN_POINT('Ctrl Pts',(27.0883372454715,4.88535378084973,334.415771031397));
#27275=CARTESIAN_POINT('Ctrl Pts',(27.0805901670936,4.86714383316806,334.279635294056));
#27276=CARTESIAN_POINT('Ctrl Pts',(27.0728430887158,4.84327396262556,334.144499920834));
#27277=CARTESIAN_POINT('Ctrl Pts',(27.06509594541,4.81940389203053,334.009363415047));
#27278=CARTESIAN_POINT('Ctrl Pts',(27.0573488021042,4.78987387195104,333.875227675017));
#27279=CARTESIAN_POINT('Ctrl Pts',(27.0496016587984,4.75479944280458,333.742595800387));
#27280=CARTESIAN_POINT('Ctrl Pts',(27.0418527737704,4.71971712818199,333.609934107296));
#27281=CARTESIAN_POINT('Ctrl Pts',(27.0341038887422,4.67908802400678,333.478777330199));
#27282=CARTESIAN_POINT('Ctrl Pts',(27.0263550037142,4.63307775098302,333.349614100931));
#27283=CARTESIAN_POINT('Ctrl Pts',(27.0185978939394,4.58701864217985,333.220313776476));
#27284=CARTESIAN_POINT('Ctrl Pts',(27.0108407841647,4.53556708638527,333.093011595494));
#27285=CARTESIAN_POINT('Ctrl Pts',(27.00308367439,4.47893736225992,332.968177377955));
#27286=CARTESIAN_POINT('Ctrl Pts',(26.9953224194638,4.4222773770207,332.843276453003));
#27287=CARTESIAN_POINT('Ctrl Pts',(26.9875611645377,4.36043388600542,332.720846468035));
#27288=CARTESIAN_POINT('Ctrl Pts',(26.9797999096115,4.29366703644942,332.601332360954));
#27289=CARTESIAN_POINT('Ctrl Pts',(26.9720262392068,4.22679338169339,332.48162707025));
#27290=CARTESIAN_POINT('Ctrl Pts',(26.9642525688022,4.15498083513406,332.364847311526));
#27291=CARTESIAN_POINT('Ctrl Pts',(26.9564788983975,4.07853323968209,332.251409511166));
#27292=CARTESIAN_POINT('Ctrl Pts',(26.9490670942204,4.00564429819054,332.143252267704));
#27293=CARTESIAN_POINT('Ctrl Pts',(26.9416552900433,3.9285422899142,332.038133080276));
#27294=CARTESIAN_POINT('Ctrl Pts',(26.9342434858662,3.84752327840411,331.936383234698));
#27295=CARTESIAN_POINT('Ctrl Pts',(26.9264684070877,3.76253328379668,331.829646326092));
#27296=CARTESIAN_POINT('Ctrl Pts',(26.9186933283094,3.67296402523994,331.726280085157));
#27297=CARTESIAN_POINT('Ctrl Pts',(26.9109182495309,3.57911269394363,331.626702594411));
#27298=CARTESIAN_POINT('Ctrl Pts',(26.9031527384819,3.48537685268535,331.527247640108));
#27299=CARTESIAN_POINT('Ctrl Pts',(26.8953872274328,3.3873696887367,331.431572441085));
#27300=CARTESIAN_POINT('Ctrl Pts',(26.8876217163838,3.28542982990655,331.340063676065));
#27301=CARTESIAN_POINT('Ctrl Pts',(26.8798639048616,3.18359104474328,331.248645642251));
#27302=CARTESIAN_POINT('Ctrl Pts',(26.8721060933393,3.07782761348009,331.161386080879));
#27303=CARTESIAN_POINT('Ctrl Pts',(26.8643482818171,2.96851609615829,331.078636047324));
#27304=CARTESIAN_POINT('Ctrl Pts',(26.8565963082941,2.85928683921914,330.995948285793));
#27305=CARTESIAN_POINT('Ctrl Pts',(26.8488443347711,2.74651512121259,330.917763532329));
#27306=CARTESIAN_POINT('Ctrl Pts',(26.841092361248,2.63061149669608,330.844393399761));
#27307=CARTESIAN_POINT('Ctrl Pts',(26.8333436706904,2.51475695743399,330.771054339488));
#27308=CARTESIAN_POINT('Ctrl Pts',(26.8255949801328,2.39577347928349,330.702526053323));
#27309=CARTESIAN_POINT('Ctrl Pts',(26.8178462895752,2.27410140653542,330.639077407785));
#27310=CARTESIAN_POINT('Ctrl Pts',(26.8100992111973,2.15245464867831,330.575641963267));
#27311=CARTESIAN_POINT('Ctrl Pts',(26.8023521328195,2.02812075524262,330.517284237823));
#27312=CARTESIAN_POINT('Ctrl Pts',(26.7946050544417,1.9015651803096,330.464227416687));
#27313=CARTESIAN_POINT('Ctrl Pts',(26.7868579111359,1.77500854471914,330.411170150884));
#27314=CARTESIAN_POINT('Ctrl Pts',(26.77911076783,1.64623055096989,330.363414029126));
#27315=CARTESIAN_POINT('Ctrl Pts',(26.7713636245242,1.51571679183518,330.321134147098));
#27316=CARTESIAN_POINT('Ctrl Pts',(26.7636147394962,1.38517369043689,330.278844759655));
#27317=CARTESIAN_POINT('Ctrl Pts',(26.7558658544681,1.25289441890203,330.242034182279));
#27318=CARTESIAN_POINT('Ctrl Pts',(26.74811696944,1.11937950503105,330.210827567709));
#27319=CARTESIAN_POINT('Ctrl Pts',(26.7403598596653,0.985722877050647,330.179587830116));
#27320=CARTESIAN_POINT('Ctrl Pts',(26.7326027498905,0.850828368059913,330.153964026328));
#27321=CARTESIAN_POINT('Ctrl Pts',(26.7248456401157,0.715207018173626,330.134030211391));
#27322=CARTESIAN_POINT('Ctrl Pts',(26.7170843851896,0.579513196574013,330.114085744461));
#27323=CARTESIAN_POINT('Ctrl Pts',(26.7093231302634,0.443092148718221,330.099837365532));
#27324=CARTESIAN_POINT('Ctrl Pts',(26.7015618753372,0.30645881297548,330.091307092672));
#27325=CARTESIAN_POINT('Ctrl Pts',(26.6937882049326,0.169606908424437,330.082763174156));
#27326=CARTESIAN_POINT('Ctrl Pts',(26.6860145345279,0.0325424283800611,
330.079955648345));
#27327=CARTESIAN_POINT('Ctrl Pts',(26.6782408641232,-0.104220018493641,
330.082854359464));
#27328=CARTESIAN_POINT('Ctrl Pts',(26.6708290599462,-0.234616140560568,
330.085618134883));
#27329=CARTESIAN_POINT('Ctrl Pts',(26.6634172557692,-0.364737428677432,
330.093568834486));
#27330=CARTESIAN_POINT('Ctrl Pts',(26.6560054515922,-0.494145080557771,
330.106636769883));
#27331=CARTESIAN_POINT('Ctrl Pts',(26.6482303728138,-0.629895386943907,
330.120345203721));
#27332=CARTESIAN_POINT('Ctrl Pts',(26.6404552940353,-0.765289329456113,
330.139728499994));
#27333=CARTESIAN_POINT('Ctrl Pts',(26.6326802152569,-0.899814506368985,
330.164762992714));
#27334=CARTESIAN_POINT('Ctrl Pts',(26.6249147042079,-1.03417414148737,330.189766678897));
#27335=CARTESIAN_POINT('Ctrl Pts',(26.6171491931589,-1.16766675754857,330.22040765392));
#27336=CARTESIAN_POINT('Ctrl Pts',(26.6093836821099,-1.29978393722895,330.256610412477));
#27337=CARTESIAN_POINT('Ctrl Pts',(26.6016258705877,-1.43177012234075,330.292777275894));
#27338=CARTESIAN_POINT('Ctrl Pts',(26.5938680590655,-1.56238321046072,330.334494845995));
#27339=CARTESIAN_POINT('Ctrl Pts',(26.5861102475433,-1.69112421338773,330.381636441618));
#27340=CARTESIAN_POINT('Ctrl Pts',(26.5783582740203,-1.81976833462812,330.428742561694));
#27341=CARTESIAN_POINT('Ctrl Pts',(26.5706063004973,-1.94654280926681,330.481264448906));
#27342=CARTESIAN_POINT('Ctrl Pts',(26.5628543269742,-2.07096342080095,330.539025490747));
#27343=CARTESIAN_POINT('Ctrl Pts',(26.5551056364166,-2.19533134013156,330.596762070752));
#27344=CARTESIAN_POINT('Ctrl Pts',(26.5473569458589,-2.31734702525195,330.659733228134));
#27345=CARTESIAN_POINT('Ctrl Pts',(26.5396082553013,-2.43654608500821,330.727714167084));
#27346=CARTESIAN_POINT('Ctrl Pts',(26.5318611769235,-2.55572034440467,330.795680962033));
#27347=CARTESIAN_POINT('Ctrl Pts',(26.5241140985457,-2.67207880475349,330.868655271766));
#27348=CARTESIAN_POINT('Ctrl Pts',(26.5163670201678,-2.78518190091799,330.946366464356));
#27349=CARTESIAN_POINT('Ctrl Pts',(26.5086198768621,-2.89828594499507,331.02407830824));
#27350=CARTESIAN_POINT('Ctrl Pts',(26.5008727335562,-3.00813424831016,331.106526892813));
#27351=CARTESIAN_POINT('Ctrl Pts',(26.4931255902504,-3.11431678705484,331.193398627073));
#27352=CARTESIAN_POINT('Ctrl Pts',(26.4853767052223,-3.22052319788898,331.280289891944));
#27353=CARTESIAN_POINT('Ctrl Pts',(26.4776278201942,-3.32306190173505,331.371606037824));
#27354=CARTESIAN_POINT('Ctrl Pts',(26.4698789351661,-3.42155679067098,331.466993887535));
#27355=CARTESIAN_POINT('Ctrl Pts',(26.4621218253913,-3.52015622309939,331.562482982896));
#27356=CARTESIAN_POINT('Ctrl Pts',(26.4543647156167,-3.61470298542498,331.66205214283));
#27357=CARTESIAN_POINT('Ctrl Pts',(26.4466076058419,-3.70485825004922,331.76531169824));
#27358=CARTESIAN_POINT('Ctrl Pts',(26.4388463509158,-3.7950616907642,331.868626432254));
#27359=CARTESIAN_POINT('Ctrl Pts',(26.4310850959895,-3.88086871341403,331.975635186401));
#27360=CARTESIAN_POINT('Ctrl Pts',(26.4233238410634,-3.96198213983656,332.08591685326));
#27361=CARTESIAN_POINT('Ctrl Pts',(26.4155501706587,-4.04322532130667,332.196374934845));
#27362=CARTESIAN_POINT('Ctrl Pts',(26.4077765002541,-4.1197596845675,332.310116066944));
#27363=CARTESIAN_POINT('Ctrl Pts',(26.4000028298494,-4.19133210397707,332.426691185133));
#27364=CARTESIAN_POINT('Ctrl Pts',(26.3925910256724,-4.25957281004351,332.537839703524));
#27365=CARTESIAN_POINT('Ctrl Pts',(26.3851792214953,-4.3233029924845,332.651564050485));
#27366=CARTESIAN_POINT('Ctrl Pts',(26.3777674173183,-4.38234379265973,332.767457515424));
#27367=CARTESIAN_POINT('Ctrl Pts',(26.3694807285346,-4.44835373098256,332.897030970559));
#27368=CARTESIAN_POINT('Ctrl Pts',(26.361194039751,-4.50868894522818,333.029682743206));
#27369=CARTESIAN_POINT('Ctrl Pts',(26.3529073509673,-4.56307101532043,333.164907094547));
#27370=CARTESIAN_POINT('Ctrl Pts',(26.3446366353416,-4.61734826026288,333.299870791727));
#27371=CARTESIAN_POINT('Ctrl Pts',(26.3363659197159,-4.66569511754526,333.437396894563));
#27372=CARTESIAN_POINT('Ctrl Pts',(26.3280952040902,-4.70787951244141,333.576956234392));
#27373=CARTESIAN_POINT('Ctrl Pts',(26.3198465163018,-4.7499515553925,333.716143878401));
#27374=CARTESIAN_POINT('Ctrl Pts',(26.3115978285134,-4.78589377748591,333.857353661482));
#27375=CARTESIAN_POINT('Ctrl Pts',(26.303349140725,-4.81552282204938,334.00003849433));
#27376=CARTESIAN_POINT('Ctrl Pts',(26.2951140627465,-4.84510298057505,334.142487906285));
#27377=CARTESIAN_POINT('Ctrl Pts',(26.2868789847679,-4.86839065493487,334.286407213762));
#27378=CARTESIAN_POINT('Ctrl Pts',(26.2786439067894,-4.88525214782621,334.431234218101));
#27379=CARTESIAN_POINT('Ctrl Pts',(26.2704270446483,-4.90207634341266,334.575740867832));
#27380=CARTESIAN_POINT('Ctrl Pts',(26.2622101825073,-4.91250266516355,334.721150901211));
#27381=CARTESIAN_POINT('Ctrl Pts',(26.2539933203662,-4.91644846050656,334.866892533332));
#27382=CARTESIAN_POINT('Ctrl Pts',(26.2515076297528,-4.91764210672796,334.910980970101));
#27383=CARTESIAN_POINT('Ctrl Pts',(26.2490219391395,-4.91824305447504,334.955099677308));
#27384=CARTESIAN_POINT('Ctrl Pts',(26.2465362485262,-4.91824994013874,334.999232650496));
#27385=CARTESIAN_POINT('',(29.7465362485277,-4.91824909912948,335.002976812401));
#27386=CARTESIAN_POINT('Ctrl Pts',(29.7465362484901,-4.91824909912908,335.002976813063));
#27387=CARTESIAN_POINT('Ctrl Pts',(29.7365654418619,-4.91814301649854,335.178245058349));
#27388=CARTESIAN_POINT('Ctrl Pts',(29.7265946352337,-4.90866871766501,335.353227704208));
#27389=CARTESIAN_POINT('Ctrl Pts',(29.7166238286055,-4.88991326132123,335.527191956743));
#27390=CARTESIAN_POINT('Ctrl Pts',(29.7088487498271,-4.87528805033922,335.662846555065));
#27391=CARTESIAN_POINT('Ctrl Pts',(29.7010736710487,-4.85499051391453,335.798106459909));
#27392=CARTESIAN_POINT('Ctrl Pts',(29.6932985922702,-4.82904777913399,335.932459441124));
#27393=CARTESIAN_POINT('Ctrl Pts',(29.6855330812212,-4.80313696854018,336.066647092442));
#27394=CARTESIAN_POINT('Ctrl Pts',(29.6777675701723,-4.77159485508092,336.199929660588));
#27395=CARTESIAN_POINT('Ctrl Pts',(29.6700020591232,-4.7345003770595,336.331799249934));
#27396=CARTESIAN_POINT('Ctrl Pts',(29.662244247601,-4.697442678321,336.463538090197));
#27397=CARTESIAN_POINT('Ctrl Pts',(29.6544864360789,-4.65484367581295,336.593866365828));
#27398=CARTESIAN_POINT('Ctrl Pts',(29.6467286245567,-4.60683341882943,336.722285955832));
#27399=CARTESIAN_POINT('Ctrl Pts',(29.6389766510337,-4.55885929108691,336.850608906022));
#27400=CARTESIAN_POINT('Ctrl Pts',(29.6312246775106,-4.50548215059201,336.977025664913));
#27401=CARTESIAN_POINT('Ctrl Pts',(29.6234727039876,-4.44688187704673,337.101053220195));
#27402=CARTESIAN_POINT('Ctrl Pts',(29.61572401343,-4.38830642075201,337.225028249734));
#27403=CARTESIAN_POINT('Ctrl Pts',(29.6079753228724,-4.32451239755108,337.346615735444));
#27404=CARTESIAN_POINT('Ctrl Pts',(29.6002266323148,-4.25572773541495,337.465352815424));
#27405=CARTESIAN_POINT('Ctrl Pts',(29.592479553937,-4.18695738450228,337.584065191163));
#27406=CARTESIAN_POINT('Ctrl Pts',(29.5847324755591,-4.11319865580338,337.699928002783));
#27407=CARTESIAN_POINT('Ctrl Pts',(29.5769853971813,-4.0347251446478,337.812503523491));
#27408=CARTESIAN_POINT('Ctrl Pts',(29.5692382538755,-3.95625097580862,337.925079987689));
#27409=CARTESIAN_POINT('Ctrl Pts',(29.5614911105697,-3.87306216921994,338.034368785366));
#27410=CARTESIAN_POINT('Ctrl Pts',(29.5537439672639,-3.78547507872997,338.139962020601));
#27411=CARTESIAN_POINT('Ctrl Pts',(29.5459950822359,-3.69786829680277,338.245578995436));
#27412=CARTESIAN_POINT('Ctrl Pts',(29.5382461972078,-3.60586151281525,338.347498453759));
#27413=CARTESIAN_POINT('Ctrl Pts',(29.5304973121797,-3.50981043676153,338.445346682193));
#27414=CARTESIAN_POINT('Ctrl Pts',(29.522740202405,-3.41365741110303,338.543298767749));
#27415=CARTESIAN_POINT('Ctrl Pts',(29.5149830926303,-3.31345179264932,338.637170711942));
#27416=CARTESIAN_POINT('Ctrl Pts',(29.5072259828555,-3.20958553062966,338.7266263274));
#27417=CARTESIAN_POINT('Ctrl Pts',(29.4994647279294,-3.10566376580051,338.816129745079));
#27418=CARTESIAN_POINT('Ctrl Pts',(29.4917034730033,-2.99807776607118,338.901211889283));
#27419=CARTESIAN_POINT('Ctrl Pts',(29.4839422180771,-2.88725063690228,338.981578433512));
#27420=CARTESIAN_POINT('Ctrl Pts',(29.4761685476724,-2.77624622044534,339.06207353802));
#27421=CARTESIAN_POINT('Ctrl Pts',(29.4683948772677,-2.66199063981317,339.137837752432));
#27422=CARTESIAN_POINT('Ctrl Pts',(29.4606212068631,-2.54493465922635,339.20862099063));
#27423=CARTESIAN_POINT('Ctrl Pts',(29.4532094026859,-2.43332766269678,339.276109252061));
#27424=CARTESIAN_POINT('Ctrl Pts',(29.4457975985088,-2.31917536817622,339.339069691241));
#27425=CARTESIAN_POINT('Ctrl Pts',(29.4383857943316,-2.2028856852926,339.397326201231));
#27426=CARTESIAN_POINT('Ctrl Pts',(29.4306107155532,-2.08089629864289,339.458438036312));
#27427=CARTESIAN_POINT('Ctrl Pts',(29.4228356367748,-1.95616919738411,339.514566300627));
#27428=CARTESIAN_POINT('Ctrl Pts',(29.4150605579963,-1.82914980680206,339.565456608793));
#27429=CARTESIAN_POINT('Ctrl Pts',(29.4072950469473,-1.70228672166639,339.616284293196));
#27430=CARTESIAN_POINT('Ctrl Pts',(29.3995295358983,-1.57313731917416,339.661886702443));
#27431=CARTESIAN_POINT('Ctrl Pts',(29.3917640248493,-1.442171417641,339.702055365969));
#27432=CARTESIAN_POINT('Ctrl Pts',(29.3840062133271,-1.31133536918059,339.742184202148));
#27433=CARTESIAN_POINT('Ctrl Pts',(29.3762484018049,-1.17868677718378,339.776889900308));
#27434=CARTESIAN_POINT('Ctrl Pts',(29.3684905902827,-1.04471489935553,339.806012259823));
#27435=CARTESIAN_POINT('Ctrl Pts',(29.3607386167597,-0.910843839614207,
339.835112703838));
#27436=CARTESIAN_POINT('Ctrl Pts',(29.3529866432367,-0.77565185657798,339.858638089672));
#27437=CARTESIAN_POINT('Ctrl Pts',(29.3452346697137,-0.639642468831033,
339.876478296329));
#27438=CARTESIAN_POINT('Ctrl Pts',(29.3374859791561,-0.503690681140176,
339.894310947647));
#27439=CARTESIAN_POINT('Ctrl Pts',(29.3297372885985,-0.366922563997023,
339.906463157758));
#27440=CARTESIAN_POINT('Ctrl Pts',(29.3219885980409,-0.229850692752224,
339.912876115021));
#27441=CARTESIAN_POINT('Ctrl Pts',(29.314241519663,-0.0928073404550829,
339.919287738014));
#27442=CARTESIAN_POINT('Ctrl Pts',(29.3064944412852,0.0445392500351959,
339.919962465052));
#27443=CARTESIAN_POINT('Ctrl Pts',(29.2987473629074,0.181672926787005,339.914893489199));
#27444=CARTESIAN_POINT('Ctrl Pts',(29.2910002196016,0.318807752850923,339.909824470863));
#27445=CARTESIAN_POINT('Ctrl Pts',(29.2832530762958,0.455729271009674,339.89901166806));
#27446=CARTESIAN_POINT('Ctrl Pts',(29.27550593299,0.591923275661444,339.882500373603));
#27447=CARTESIAN_POINT('Ctrl Pts',(29.2677570479619,0.728147899616939,339.865985367055));
#27448=CARTESIAN_POINT('Ctrl Pts',(29.2600081629338,0.863644296641082,339.843769366557));
#27449=CARTESIAN_POINT('Ctrl Pts',(29.2522592779057,0.99790570809472,339.81594925848));
#27450=CARTESIAN_POINT('Ctrl Pts',(29.2445021681309,1.13230962599766,339.788099621852));
#27451=CARTESIAN_POINT('Ctrl Pts',(29.2367450583561,1.26547555648274,339.754634074876));
#27452=CARTESIAN_POINT('Ctrl Pts',(29.2289879485814,1.39690868619675,339.71570028574));
#27453=CARTESIAN_POINT('Ctrl Pts',(29.2212266936553,1.52841204957296,339.676745691632));
#27454=CARTESIAN_POINT('Ctrl Pts',(29.2134654387291,1.65818039751886,339.632317159454));
#27455=CARTESIAN_POINT('Ctrl Pts',(29.2057041838029,1.78573725795884,339.582611210657));
#27456=CARTESIAN_POINT('Ctrl Pts',(29.1979305133983,1.91349816780484,339.53282574854));
#27457=CARTESIAN_POINT('Ctrl Pts',(29.1901568429936,2.03904016272585,339.477746157018));
#27458=CARTESIAN_POINT('Ctrl Pts',(29.182383172589,2.16190900558718,339.417616157393));
#27459=CARTESIAN_POINT('Ctrl Pts',(29.1749713684119,2.27905827425294,339.360285223717));
#27460=CARTESIAN_POINT('Ctrl Pts',(29.1675595642347,2.39377740738313,339.298363630232));
#27461=CARTESIAN_POINT('Ctrl Pts',(29.1601477600576,2.50569756959003,339.232099095278));
#27462=CARTESIAN_POINT('Ctrl Pts',(29.1523726812792,2.62310327233956,339.162586738073));
#27463=CARTESIAN_POINT('Ctrl Pts',(29.1445976025008,2.73779971857641,339.088075282148));
#27464=CARTESIAN_POINT('Ctrl Pts',(29.1368225237223,2.84933194502609,339.008801632602));
#27465=CARTESIAN_POINT('Ctrl Pts',(29.1290570126733,2.96072692397064,338.929625534329));
#27466=CARTESIAN_POINT('Ctrl Pts',(29.1212915016242,3.06896511507072,338.8456991268));
#27467=CARTESIAN_POINT('Ctrl Pts',(29.1135259905752,3.17361696533209,338.757304674878));
#27468=CARTESIAN_POINT('Ctrl Pts',(29.105768179053,3.27816505297931,338.668997866311));
#27469=CARTESIAN_POINT('Ctrl Pts',(29.0980103675308,3.37913357947951,338.576232080054));
#27470=CARTESIAN_POINT('Ctrl Pts',(29.0902525560086,3.47612306329126,338.479332049597));
#27471=CARTESIAN_POINT('Ctrl Pts',(29.0825005824856,3.57303955944059,338.382504939487));
#27472=CARTESIAN_POINT('Ctrl Pts',(29.0747486089626,3.66598269761639,338.281550052918));
#27473=CARTESIAN_POINT('Ctrl Pts',(29.0669966354396,3.75458739192506,338.176831216621));
#27474=CARTESIAN_POINT('Ctrl Pts',(29.059247944882,3.84315456209309,338.072156728813));
#27475=CARTESIAN_POINT('Ctrl Pts',(29.0514992543243,3.92738669077012,337.963721759472));
#27476=CARTESIAN_POINT('Ctrl Pts',(29.0437505637667,4.00695693805955,337.851925517793));
#27477=CARTESIAN_POINT('Ctrl Pts',(29.0360034853889,4.08651063009445,337.740152536255));
#27478=CARTESIAN_POINT('Ctrl Pts',(29.028256407011,4.16140414351533,337.625019991667));
#27479=CARTESIAN_POINT('Ctrl Pts',(29.0205093286332,4.23135243479777,337.506958243575));
#27480=CARTESIAN_POINT('Ctrl Pts',(29.0127621853274,4.30130131231427,337.388895506013));
#27481=CARTESIAN_POINT('Ctrl Pts',(29.0050150420216,4.36630468578707,337.267903852266));
#27482=CARTESIAN_POINT('Ctrl Pts',(28.9972678987158,4.42612237675188,337.144440199333));
#27483=CARTESIAN_POINT('Ctrl Pts',(28.9895190136877,4.48595351600351,337.02094878915));
#27484=CARTESIAN_POINT('Ctrl Pts',(28.9817701286596,4.54059648243839,336.894984625581));
#27485=CARTESIAN_POINT('Ctrl Pts',(28.9740212436315,4.58985851369572,336.76702628355));
#27486=CARTESIAN_POINT('Ctrl Pts',(28.9662641338568,4.63917283218208,336.638932125212));
#27487=CARTESIAN_POINT('Ctrl Pts',(28.9585070240821,4.68309466581821,336.508839925575));
#27488=CARTESIAN_POINT('Ctrl Pts',(28.9507499143074,4.72148042003775,336.377245695473));
#27489=CARTESIAN_POINT('Ctrl Pts',(28.9429886593812,4.75988668637704,336.245581145623));
#27490=CARTESIAN_POINT('Ctrl Pts',(28.935227404455,4.79275088500713,336.112413345279));
#27491=CARTESIAN_POINT('Ctrl Pts',(28.9274661495288,4.81998042862848,335.978249319007));
#27492=CARTESIAN_POINT('Ctrl Pts',(28.9196924791241,4.8472535306455,335.843870674018));
#27493=CARTESIAN_POINT('Ctrl Pts',(28.9119188087195,4.86887390411284,335.708493004729));
#27494=CARTESIAN_POINT('Ctrl Pts',(28.9041451383148,4.88480068569567,335.572630180419));
#27495=CARTESIAN_POINT('Ctrl Pts',(28.8967333341378,4.8999860717639,335.443091803269));
#27496=CARTESIAN_POINT('Ctrl Pts',(28.8893215299608,4.90999598828242,335.313112709501));
#27497=CARTESIAN_POINT('Ctrl Pts',(28.8819097257838,4.914839148895,335.183137115269));
#27498=CARTESIAN_POINT('Ctrl Pts',(28.8741346470054,4.91991968723628,335.046791029985));
#27499=CARTESIAN_POINT('Ctrl Pts',(28.8663595682269,4.91933024265626,334.910017917136));
#27500=CARTESIAN_POINT('Ctrl Pts',(28.8585844894485,4.91302382697354,334.773328567988));
#27501=CARTESIAN_POINT('Ctrl Pts',(28.8508189783995,4.9067251717368,334.636807423787));
#27502=CARTESIAN_POINT('Ctrl Pts',(28.8430534673505,4.89472356106533,334.500370224921));
#27503=CARTESIAN_POINT('Ctrl Pts',(28.8352879563015,4.87702390172891,334.364530941379));
#27504=CARTESIAN_POINT('Ctrl Pts',(28.8275301447793,4.85934179165624,334.228826342882));
#27505=CARTESIAN_POINT('Ctrl Pts',(28.8197723332571,4.83597292618353,334.093718865036));
#27506=CARTESIAN_POINT('Ctrl Pts',(28.8120145217349,4.80697419824712,333.959720172316));
#27507=CARTESIAN_POINT('Ctrl Pts',(28.8042625482119,4.77799729277312,333.825822317862));
#27508=CARTESIAN_POINT('Ctrl Pts',(28.7965105746889,4.74339904002279,333.693031968203));
#27509=CARTESIAN_POINT('Ctrl Pts',(28.7887586011659,4.70328782072906,333.561853019375));
#27510=CARTESIAN_POINT('Ctrl Pts',(28.7810099106083,4.66319358856045,333.430729624909));
#27511=CARTESIAN_POINT('Ctrl Pts',(28.7732612200507,4.61759114754874,333.301216646983));
#27512=CARTESIAN_POINT('Ctrl Pts',(28.765512529493,4.56663932940033,333.173804967241));
#27513=CARTESIAN_POINT('Ctrl Pts',(28.7577654511152,4.51569811220324,333.046419796563));
#27514=CARTESIAN_POINT('Ctrl Pts',(28.7500183727374,4.45940987671494,332.921135417163));
#27515=CARTESIAN_POINT('Ctrl Pts',(28.7422712943596,4.39798226805332,332.798424420469));
#27516=CARTESIAN_POINT('Ctrl Pts',(28.7345241510538,4.33655414456926,332.675712395338));
#27517=CARTESIAN_POINT('Ctrl Pts',(28.726777007748,4.26998673696837,332.555574145456));
#27518=CARTESIAN_POINT('Ctrl Pts',(28.7190298644422,4.19853430215554,332.438458906025));
#27519=CARTESIAN_POINT('Ctrl Pts',(28.7112809794141,4.12706580331839,332.321317336601));
#27520=CARTESIAN_POINT('Ctrl Pts',(28.703532094386,4.05071029539571,332.20720046364));
#27521=CARTESIAN_POINT('Ctrl Pts',(28.6957832093579,3.96976590747842,332.096529369475));
#27522=CARTESIAN_POINT('Ctrl Pts',(28.6880260995831,3.88873560435148,331.985740807867));
#27523=CARTESIAN_POINT('Ctrl Pts',(28.6802689898084,3.80310692269607,331.878405647019));
#27524=CARTESIAN_POINT('Ctrl Pts',(28.6725118800337,3.71321926134677,331.774913058588));
#27525=CARTESIAN_POINT('Ctrl Pts',(28.6647506251075,3.62328356690523,331.671365167028));
#27526=CARTESIAN_POINT('Ctrl Pts',(28.6569893701814,3.52908462621157,331.57166422334));
#27527=CARTESIAN_POINT('Ctrl Pts',(28.6492281152552,3.43099870274052,331.476162466246));
#27528=CARTESIAN_POINT('Ctrl Pts',(28.6414544448505,3.33275587375803,331.380507937465));
#27529=CARTESIAN_POINT('Ctrl Pts',(28.6336807744458,3.23061392815709,331.289066279344));
#27530=CARTESIAN_POINT('Ctrl Pts',(28.6259071040412,3.12498287608195,331.202149938887));
#27531=CARTESIAN_POINT('Ctrl Pts',(28.6184952998641,3.02426897489412,331.119279574989));
#27532=CARTESIAN_POINT('Ctrl Pts',(28.611083495687,2.92038372215826,331.040522876799));
#27533=CARTESIAN_POINT('Ctrl Pts',(28.6036716915099,2.81370538416739,330.966112907677));
#27534=CARTESIAN_POINT('Ctrl Pts',(28.5958966127315,2.7017984230533,330.888055884313));
#27535=CARTESIAN_POINT('Ctrl Pts',(28.588121533953,2.58646401224734,330.814535781434));
#27536=CARTESIAN_POINT('Ctrl Pts',(28.5803464551746,2.46810625902171,330.745868530866));
#27537=CARTESIAN_POINT('Ctrl Pts',(28.5725809441256,2.34989415254644,330.677285779721));
#27538=CARTESIAN_POINT('Ctrl Pts',(28.5648154330765,2.22866644107313,330.613544193107));
#27539=CARTESIAN_POINT('Ctrl Pts',(28.5570499220275,2.10485798826539,330.554917783467));
#27540=CARTESIAN_POINT('Ctrl Pts',(28.5492921105053,1.98117229189897,330.496349502084));
#27541=CARTESIAN_POINT('Ctrl Pts',(28.5415342989831,1.85491129737371,330.442886470885));
#27542=CARTESIAN_POINT('Ctrl Pts',(28.5337764874609,1.72653606229579,330.394757738393));
#27543=CARTESIAN_POINT('Ctrl Pts',(28.5260245139379,1.59825743365327,330.346665224299));
#27544=CARTESIAN_POINT('Ctrl Pts',(28.5182725404149,1.46786809585616,330.303899155449));
#27545=CARTESIAN_POINT('Ctrl Pts',(28.5105205668918,1.33585043686496,330.266641079231));
#27546=CARTESIAN_POINT('Ctrl Pts',(28.5027718763342,1.2038886874309,330.22939878183));
#27547=CARTESIAN_POINT('Ctrl Pts',(28.4950231857766,1.07030036375591,330.197659943553));
#27548=CARTESIAN_POINT('Ctrl Pts',(28.487274495219,0.935584211636791,330.171556643655));
#27549=CARTESIAN_POINT('Ctrl Pts',(28.4795274168411,0.80089608833811,330.145458774765));
#27550=CARTESIAN_POINT('Ctrl Pts',(28.4717803384633,0.665080986835005,330.124994186335));
#27551=CARTESIAN_POINT('Ctrl Pts',(28.4640332600854,0.528648688027829,330.110244011492));
#27552=CARTESIAN_POINT('Ctrl Pts',(28.4562861167796,0.392215245786766,330.095493713029));
#27553=CARTESIAN_POINT('Ctrl Pts',(28.4485389734738,0.25516498453403,330.086457965692));
#27554=CARTESIAN_POINT('Ctrl Pts',(28.440791830168,0.118013268734895,330.083166066369));
#27555=CARTESIAN_POINT('Ctrl Pts',(28.4330429451399,-0.0191692816817649,
330.079873426958));
#27556=CARTESIAN_POINT('Ctrl Pts',(28.4252940601118,-0.156452941347069,
330.082327214559));
#27557=CARTESIAN_POINT('Ctrl Pts',(28.4175451750837,-0.293322278384767,
330.090504597873));
#27558=CARTESIAN_POINT('Ctrl Pts',(28.409788065309,-0.430336889950923,330.098690660746));
#27559=CARTESIAN_POINT('Ctrl Pts',(28.4020309555342,-0.566935909620196,
330.112612431533));
#27560=CARTESIAN_POINT('Ctrl Pts',(28.3942738457595,-0.702608406458019,
330.132195105628));
#27561=CARTESIAN_POINT('Ctrl Pts',(28.3865125908333,-0.838353402340095,
330.151788244077));
#27562=CARTESIAN_POINT('Ctrl Pts',(28.3787513359072,-0.973170504857078,
330.177048241484));
#27563=CARTESIAN_POINT('Ctrl Pts',(28.370990080981,-1.10655989119709,330.20784930645));
#27564=CARTESIAN_POINT('Ctrl Pts',(28.3632164105763,-1.24016265708392,330.238699643081));
#27565=CARTESIAN_POINT('Ctrl Pts',(28.3554427401717,-1.3723327658881,330.27510865611));
#27566=CARTESIAN_POINT('Ctrl Pts',(28.347669069767,-1.50258559424392,330.316900642259));
#27567=CARTESIAN_POINT('Ctrl Pts',(28.3402572655899,-1.62677512210242,330.356747201399));
#27568=CARTESIAN_POINT('Ctrl Pts',(28.3328454614129,-1.74922158100058,330.40148675827));
#27569=CARTESIAN_POINT('Ctrl Pts',(28.3254336572358,-1.86952428139009,330.450927344635));
#27570=CARTESIAN_POINT('Ctrl Pts',(28.3176585784574,-1.99572337548938,330.502791161413));
#27571=CARTESIAN_POINT('Ctrl Pts',(28.3098834996789,-2.11996206605793,330.55999238176));
#27572=CARTESIAN_POINT('Ctrl Pts',(28.3021084209005,-2.24175599364902,330.622362152092));
#27573=CARTESIAN_POINT('Ctrl Pts',(28.2943429098514,-2.36340004605827,330.68465517245));
#27574=CARTESIAN_POINT('Ctrl Pts',(28.2865773988024,-2.48260497683239,330.752103911299));
#27575=CARTESIAN_POINT('Ctrl Pts',(28.2788118877534,-2.59890503337951,330.824490966364));
#27576=CARTESIAN_POINT('Ctrl Pts',(28.2710540762312,-2.71508977808188,330.896806249453));
#27577=CARTESIAN_POINT('Ctrl Pts',(28.263296264709,-2.82837505059285,330.97404989952));
#27578=CARTESIAN_POINT('Ctrl Pts',(28.2555384531868,-2.93831873439641,331.055958154685));
#27579=CARTESIAN_POINT('Ctrl Pts',(28.2477864796638,-3.04817968209153,331.137804771291));
#27580=CARTESIAN_POINT('Ctrl Pts',(28.2400345061408,-3.15470373418234,331.224308773408));
#27581=CARTESIAN_POINT('Ctrl Pts',(28.2322825326177,-3.25747717579205,331.315162756417));
#27582=CARTESIAN_POINT('Ctrl Pts',(28.2245338420601,-3.36020709278808,331.405978262711));
#27583=CARTESIAN_POINT('Ctrl Pts',(28.2167851515025,-3.45918926625015,331.501139827506));
#27584=CARTESIAN_POINT('Ctrl Pts',(28.2090364609448,-3.55404272794733,331.600299520483));
#27585=CARTESIAN_POINT('Ctrl Pts',(28.201289382567,-3.64887645458957,331.699438582459));
#27586=CARTESIAN_POINT('Ctrl Pts',(28.1935423041892,-3.73958290808541,331.802573835744));
#27587=CARTESIAN_POINT('Ctrl Pts',(28.1857952258113,-3.82581799015994,331.909320500494));
#27588=CARTESIAN_POINT('Ctrl Pts',(28.1780480825055,-3.91205379496752,332.016068059884));
#27589=CARTESIAN_POINT('Ctrl Pts',(28.1703009391997,-3.99381790797882,332.126426787055));
#27590=CARTESIAN_POINT('Ctrl Pts',(28.1625537958939,-4.0708067995312,332.239979155262));
#27591=CARTESIAN_POINT('Ctrl Pts',(28.1548049108658,-4.14781299982081,332.353557052451));
#27592=CARTESIAN_POINT('Ctrl Pts',(28.1470560258377,-4.22004162305708,332.470329695952));
#27593=CARTESIAN_POINT('Ctrl Pts',(28.1393071408096,-4.28723293880348,332.589851292775));
#27594=CARTESIAN_POINT('Ctrl Pts',(28.1315500310349,-4.35449557210673,332.709499751056));
#27595=CARTESIAN_POINT('Ctrl Pts',(28.1237929212601,-4.41671002563736,332.831902649912));
#27596=CARTESIAN_POINT('Ctrl Pts',(28.1160358114854,-4.47366271013816,332.956589855555));
#27597=CARTESIAN_POINT('Ctrl Pts',(28.1082745565592,-4.5306458283326,333.081343690054));
#27598=CARTESIAN_POINT('Ctrl Pts',(28.1005133016331,-4.58236142759018,333.208383901773));
#27599=CARTESIAN_POINT('Ctrl Pts',(28.0927520467069,-4.62864480577895,333.337222106102));
#27600=CARTESIAN_POINT('Ctrl Pts',(28.0849783763022,-4.67500222228903,333.466266409569));
#27601=CARTESIAN_POINT('Ctrl Pts',(28.0772047058975,-4.71590993627412,333.597114079887));
#27602=CARTESIAN_POINT('Ctrl Pts',(28.0694310354928,-4.75125344285673,333.729262503803));
#27603=CARTESIAN_POINT('Ctrl Pts',(28.0620192313158,-4.78495170070443,333.855259386791));
#27604=CARTESIAN_POINT('Ctrl Pts',(28.0546074271388,-4.81359205774079,333.982438367736));
#27605=CARTESIAN_POINT('Ctrl Pts',(28.0471956229618,-4.83711910804647,334.11035861322));
#27606=CARTESIAN_POINT('Ctrl Pts',(28.0354721385041,-4.87433258562982,334.312694100496));
#27607=CARTESIAN_POINT('Ctrl Pts',(28.0237486540465,-4.89885879954496,334.517429559264));
#27608=CARTESIAN_POINT('Ctrl Pts',(28.0120251695888,-4.91045911773521,334.723279354671));
#27609=CARTESIAN_POINT('Ctrl Pts',(28.0068621958893,-4.91556784952385,334.813934746725));
#27610=CARTESIAN_POINT('Ctrl Pts',(28.0016992221897,-4.91817014931963,334.904805934471));
#27611=CARTESIAN_POINT('Ctrl Pts',(27.9965362484901,-4.91824819040101,334.995780981491));
#27612=CARTESIAN_POINT('',(31.49653624844,-4.91824929754497,335.002628630519));
#27613=CARTESIAN_POINT('Ctrl Pts',(31.4965362484401,-4.91824929754497,335.002628630519));
#27614=CARTESIAN_POINT('Ctrl Pts',(31.4879704571182,-4.91816808857999,335.154573124847));
#27615=CARTESIAN_POINT('Ctrl Pts',(31.4794046657963,-4.91104154518577,335.30627050863));
#27616=CARTESIAN_POINT('Ctrl Pts',(31.4708388744744,-4.89696263499547,335.457099566788));
#27617=CARTESIAN_POINT('Ctrl Pts',(31.4622260458395,-4.88280641331326,335.608756872258));
#27618=CARTESIAN_POINT('Ctrl Pts',(31.4536132172045,-4.86162134728139,335.759536059089));
#27619=CARTESIAN_POINT('Ctrl Pts',(31.4450003885695,-4.8335521266272,335.908821710611));
#27620=CARTESIAN_POINT('Ctrl Pts',(31.4363631848292,-4.80540346747042,336.058529854398));
#27621=CARTESIAN_POINT('Ctrl Pts',(31.4277259810889,-4.77033175083558,336.206735782444));
#27622=CARTESIAN_POINT('Ctrl Pts',(31.4190887773486,-4.72853164846848,336.352838316996));
#27623=CARTESIAN_POINT('Ctrl Pts',(31.4104202046795,-4.6865797348817,336.499471472353));
#27624=CARTESIAN_POINT('Ctrl Pts',(31.4017516320105,-4.63785059343201,336.643985718313));
#27625=CARTESIAN_POINT('Ctrl Pts',(31.3930830593414,-4.5825882820768,336.785796096835));
#27626=CARTESIAN_POINT('Ctrl Pts',(31.3907393843106,-4.56764731033793,336.824136600622));
#27627=CARTESIAN_POINT('Ctrl Pts',(31.3883957092799,-4.55222904365927,336.862279597944));
#27628=CARTESIAN_POINT('Ctrl Pts',(31.3860520342491,-4.53633887755892,336.900213843347));
#27629=CARTESIAN_POINT('Ctrl Pts',(31.3782769554707,-4.48362367958517,337.026059680564));
#27630=CARTESIAN_POINT('Ctrl Pts',(31.3705018766923,-4.42558444376334,337.149909101025));
#27631=CARTESIAN_POINT('Ctrl Pts',(31.3627267979138,-4.36239329201938,337.271278897063));
#27632=CARTESIAN_POINT('Ctrl Pts',(31.3549612868648,-4.29927990101051,337.392499339841));
#27633=CARTESIAN_POINT('Ctrl Pts',(31.3471957758158,-4.23102738716775,337.511245886095));
#27634=CARTESIAN_POINT('Ctrl Pts',(31.3394302647668,-4.15785629429548,337.62705426257));
#27635=CARTESIAN_POINT('Ctrl Pts',(31.3316724532446,-4.08475775077477,337.742747814702));
#27636=CARTESIAN_POINT('Ctrl Pts',(31.3239146417224,-4.00675054074156,337.855508666182));
#27637=CARTESIAN_POINT('Ctrl Pts',(31.3161568302002,-3.92410140686709,337.964896492481));
#27638=CARTESIAN_POINT('Ctrl Pts',(31.3084048566772,-3.84151446908704,338.074202000971));
#27639=CARTESIAN_POINT('Ctrl Pts',(31.3006528831542,-3.75429279518361,338.18013922605));
#27640=CARTESIAN_POINT('Ctrl Pts',(31.2929009096312,-3.66274657769866,338.282296539019));
#27641=CARTESIAN_POINT('Ctrl Pts',(31.2851522190736,-3.57123913009104,338.384410588306));
#27642=CARTESIAN_POINT('Ctrl Pts',(31.2774035285159,-3.47541104183568,338.482747618863));
#27643=CARTESIAN_POINT('Ctrl Pts',(31.2696548379583,-3.37561280902233,338.57692902167));
#27644=CARTESIAN_POINT('Ctrl Pts',(31.2619077595805,-3.27583534006499,338.671090829249));
#27645=CARTESIAN_POINT('Ctrl Pts',(31.2541606812027,-3.17208965366063,338.76109846075));
#27646=CARTESIAN_POINT('Ctrl Pts',(31.2464136028248,-3.06476284550104,338.84661042521));
#27647=CARTESIAN_POINT('Ctrl Pts',(31.238666459519,-2.95743513783943,338.932123106343));
#27648=CARTESIAN_POINT('Ctrl Pts',(31.2309193162132,-2.84652655426544,339.013139801715));
#27649=CARTESIAN_POINT('Ctrl Pts',(31.2231721729074,-2.7324566625561,339.08935980928));
#27650=CARTESIAN_POINT('Ctrl Pts',(31.2154232878793,-2.61836112551333,339.16559695272));
#27651=CARTESIAN_POINT('Ctrl Pts',(31.2076744028513,-2.50110319099887,339.237035045346));
#27652=CARTESIAN_POINT('Ctrl Pts',(31.1999255178232,-2.38113039649116,339.303417374298));
#27653=CARTESIAN_POINT('Ctrl Pts',(31.1921684080485,-2.2610302616198,339.369870162138));
#27654=CARTESIAN_POINT('Ctrl Pts',(31.1844112982737,-2.13820985307904,339.431256277199));
#27655=CARTESIAN_POINT('Ctrl Pts',(31.176654188499,-2.01314073687532,339.487365311186));
#27656=CARTESIAN_POINT('Ctrl Pts',(31.1688929335728,-1.88800478773475,339.543504328046));
#27657=CARTESIAN_POINT('Ctrl Pts',(31.1611316786467,-1.76061809939056,339.594360500068));
#27658=CARTESIAN_POINT('Ctrl Pts',(31.1533704237205,-1.63147015798782,339.639772428266));
#27659=CARTESIAN_POINT('Ctrl Pts',(31.1455967533159,-1.50211562196822,339.685257000748));
#27660=CARTESIAN_POINT('Ctrl Pts',(31.1378230829112,-1.37099457687206,339.725279812042));
#27661=CARTESIAN_POINT('Ctrl Pts',(31.1300494125065,-1.23861039804341,339.759729755391));
#27662=CARTESIAN_POINT('Ctrl Pts',(31.1226376083294,-1.11238873458886,339.79257604559));
#27663=CARTESIAN_POINT('Ctrl Pts',(31.1152258041524,-0.985019169873967,
339.820356564486));
#27664=CARTESIAN_POINT('Ctrl Pts',(31.1078139999753,-0.856942901563595,
339.843018885567));
#27665=CARTESIAN_POINT('Ctrl Pts',(31.1000389211969,-0.722589233823908,
339.866791954512));
#27666=CARTESIAN_POINT('Ctrl Pts',(31.0922638424184,-0.587033253152717,
339.885007550787));
#27667=CARTESIAN_POINT('Ctrl Pts',(31.08448876364,-0.450774444236788,339.897548923995));
#27668=CARTESIAN_POINT('Ctrl Pts',(31.0767232525909,-0.314683310459706,
339.910074864245));
#27669=CARTESIAN_POINT('Ctrl Pts',(31.068957741542,-0.17789145479916,339.916940439105));
#27670=CARTESIAN_POINT('Ctrl Pts',(31.061192230493,-0.0409086434484924,
339.918079863665));
#27671=CARTESIAN_POINT('Ctrl Pts',(31.0534344189708,0.095938349045814,339.919218158483));
#27672=CARTESIAN_POINT('Ctrl Pts',(31.0456766074485,0.232975532103677,339.914641598307));
#27673=CARTESIAN_POINT('Ctrl Pts',(31.0379187959263,0.369688277670826,339.904336207873));
#27674=CARTESIAN_POINT('Ctrl Pts',(31.0301668224034,0.506298142561153,339.894038572571));
#27675=CARTESIAN_POINT('Ctrl Pts',(31.0224148488803,0.642583667729312,339.87802071736));
#27676=CARTESIAN_POINT('Ctrl Pts',(31.0146628753573,0.778030842837607,339.856320733857));
#27677=CARTESIAN_POINT('Ctrl Pts',(31.0069141847997,0.913420655987198,339.83462994031));
#27678=CARTESIAN_POINT('Ctrl Pts',(30.9991654942421,1.04797244008067,339.807261866306));
#27679=CARTESIAN_POINT('Ctrl Pts',(30.9914168036845,1.18117814117006,339.774306364418));
#27680=CARTESIAN_POINT('Ctrl Pts',(30.9836697253067,1.31435612770079,339.741357719197));
#27681=CARTESIAN_POINT('Ctrl Pts',(30.9759226469288,1.44618820909791,339.702824052225));
#27682=CARTESIAN_POINT('Ctrl Pts',(30.968175568551,1.57617773863676,339.658846080171));
#27683=CARTESIAN_POINT('Ctrl Pts',(30.9604284252452,1.70616835761289,339.61486773954));
#27684=CARTESIAN_POINT('Ctrl Pts',(30.9526812819394,1.83431602367146,339.565445128084));
#27685=CARTESIAN_POINT('Ctrl Pts',(30.9449341386336,1.96014081784816,339.510768342168));
#27686=CARTESIAN_POINT('Ctrl Pts',(30.9371852536055,2.08599390010994,339.456079263749));
#27687=CARTESIAN_POINT('Ctrl Pts',(30.9294363685774,2.20952271288873,339.396133816065));
#27688=CARTESIAN_POINT('Ctrl Pts',(30.9216874835493,2.33026919265421,339.331169420869));
#27689=CARTESIAN_POINT('Ctrl Pts',(30.9139303737746,2.45114383398085,339.266136071792));
#27690=CARTESIAN_POINT('Ctrl Pts',(30.9061732639998,2.56922989824594,339.196073319186));
#27691=CARTESIAN_POINT('Ctrl Pts',(30.8984161542251,2.68409525720108,339.121263848963));
#27692=CARTESIAN_POINT('Ctrl Pts',(30.8906548992989,2.79902199653145,339.046414402952));
#27693=CARTESIAN_POINT('Ctrl Pts',(30.8828936443728,2.91072428306379,338.966813411855));
#27694=CARTESIAN_POINT('Ctrl Pts',(30.8751323894466,3.01880150390626,338.882785152763));
#27695=CARTESIAN_POINT('Ctrl Pts',(30.867358719042,3.12705161307979,338.79862247584));
#27696=CARTESIAN_POINT('Ctrl Pts',(30.8595850486373,3.23166477017122,338.710018631373));
#27697=CARTESIAN_POINT('Ctrl Pts',(30.8518113782326,3.3322751378583,338.617336792187));
#27698=CARTESIAN_POINT('Ctrl Pts',(30.8443995740555,3.42820206872423,338.528969314913));
#27699=CARTESIAN_POINT('Ctrl Pts',(30.8369877698784,3.52049027966644,338.436895163454));
#27700=CARTESIAN_POINT('Ctrl Pts',(30.8295759657013,3.6088569267407,338.341456979345));
#27701=CARTESIAN_POINT('Ctrl Pts',(30.8218008869229,3.70155468641853,338.241341085538));
#27702=CARTESIAN_POINT('Ctrl Pts',(30.8140258081444,3.79022968928016,338.137206673786));
#27703=CARTESIAN_POINT('Ctrl Pts',(30.806250729366,3.87451345760266,338.029410591081));
#27704=CARTESIAN_POINT('Ctrl Pts',(30.798485218317,3.95869350938259,337.921747158319));
#27705=CARTESIAN_POINT('Ctrl Pts',(30.790719707268,4.03849283996574,337.810431325071));
#27706=CARTESIAN_POINT('Ctrl Pts',(30.782954196219,4.11358026568129,337.695856164616));
#27707=CARTESIAN_POINT('Ctrl Pts',(30.7751963846968,4.18859324199559,337.581394605766));
#27708=CARTESIAN_POINT('Ctrl Pts',(30.7674385731746,4.25890339785153,337.463680475659));
#27709=CARTESIAN_POINT('Ctrl Pts',(30.7596807616524,4.32422048638134,337.343138973185));
#27710=CARTESIAN_POINT('Ctrl Pts',(30.7519287881294,4.38948842173062,337.222688182015));
#27711=CARTESIAN_POINT('Ctrl Pts',(30.7441768146064,4.44977058328796,337.099414595818));
#27712=CARTESIAN_POINT('Ctrl Pts',(30.7364248410834,4.50482084261996,336.973771070412));
#27713=CARTESIAN_POINT('Ctrl Pts',(30.7286761505257,4.55984778813452,336.848180755114));
#27714=CARTESIAN_POINT('Ctrl Pts',(30.7209274599681,4.60964708178462,336.72022285411));
#27715=CARTESIAN_POINT('Ctrl Pts',(30.7131787694105,4.65401934537325,336.590373225187));
#27716=CARTESIAN_POINT('Ctrl Pts',(30.7054316910327,4.69838237694183,336.460550612564));
#27717=CARTESIAN_POINT('Ctrl Pts',(30.6976846126548,4.73732049807176,336.328837424542));
#27718=CARTESIAN_POINT('Ctrl Pts',(30.689937534277,4.77068327637423,336.195727451815));
#27719=CARTESIAN_POINT('Ctrl Pts',(30.6821903909712,4.80404633428892,336.062616363497));
#27720=CARTESIAN_POINT('Ctrl Pts',(30.6744432476654,4.83183386114659,335.92810884627));
#27721=CARTESIAN_POINT('Ctrl Pts',(30.6666961043596,4.85394600134562,335.79271134628));
#27722=CARTESIAN_POINT('Ctrl Pts',(30.6589472193315,4.87606311282318,335.657283406057));
#27723=CARTESIAN_POINT('Ctrl Pts',(30.6511983343034,4.89250223566147,335.520965470609));
#27724=CARTESIAN_POINT('Ctrl Pts',(30.6434494492753,4.90321513841902,335.384271217864));
#27725=CARTESIAN_POINT('Ctrl Pts',(30.6356923395006,4.91393941196226,335.247431876427));
#27726=CARTESIAN_POINT('Ctrl Pts',(30.6279352297258,4.91892529372301,335.110215810095));
#27727=CARTESIAN_POINT('Ctrl Pts',(30.6201781199511,4.91817665092632,334.973139382301));
#27728=CARTESIAN_POINT('Ctrl Pts',(30.6124168650249,4.91742760807885,334.835989705246));
#27729=CARTESIAN_POINT('Ctrl Pts',(30.6046556100988,4.9109379531716,334.698980205651));
#27730=CARTESIAN_POINT('Ctrl Pts',(30.5968943551726,4.89876358310378,334.562623252383));
#27731=CARTESIAN_POINT('Ctrl Pts',(30.5891206847679,4.88656973801147,334.426048172428));
#27732=CARTESIAN_POINT('Ctrl Pts',(30.5813470143632,4.86867305692279,334.290128112477));
#27733=CARTESIAN_POINT('Ctrl Pts',(30.5735733439585,4.84518096404822,334.155367246595));
#27734=CARTESIAN_POINT('Ctrl Pts',(30.5661615397815,4.82278243374894,334.026879531441));
#27735=CARTESIAN_POINT('Ctrl Pts',(30.5587497356045,4.79529776190851,333.89944579941));
#27736=CARTESIAN_POINT('Ctrl Pts',(30.5513379314274,4.76286202001619,333.773489323003));
#27737=CARTESIAN_POINT('Ctrl Pts',(30.543562852649,4.72883650579246,333.641359344482));
#27738=CARTESIAN_POINT('Ctrl Pts',(30.5357877738705,4.68925478955925,333.510437537347));
#27739=CARTESIAN_POINT('Ctrl Pts',(30.5280126950921,4.64421754712508,333.38122687276));
#27740=CARTESIAN_POINT('Ctrl Pts',(30.5202471840431,4.59923572588494,333.252175210121));
#27741=CARTESIAN_POINT('Ctrl Pts',(30.512481672994,4.54881186355072,333.124830865918));
#27742=CARTESIAN_POINT('Ctrl Pts',(30.504716161945,4.49309728134059,332.99968505407));
#27743=CARTESIAN_POINT('Ctrl Pts',(30.4969583504228,4.43743794030096,332.874663324659));
#27744=CARTESIAN_POINT('Ctrl Pts',(30.4892005389006,4.37649847670219,332.751836144362));
#27745=CARTESIAN_POINT('Ctrl Pts',(30.4814427273784,4.31047938012951,332.63167768748));
#27746=CARTESIAN_POINT('Ctrl Pts',(30.4736907538554,4.24450996502058,332.511609653648));
#27747=CARTESIAN_POINT('Ctrl Pts',(30.4659387803324,4.1734687130689,332.394206687002));
#27748=CARTESIAN_POINT('Ctrl Pts',(30.4581868068094,4.09760324617584,332.279920828463));
#27749=CARTESIAN_POINT('Ctrl Pts',(30.4504381162518,4.02176990835305,332.165683370053));
#27750=CARTESIAN_POINT('Ctrl Pts',(30.4426894256942,3.94111663481345,332.054560719145));
#27751=CARTESIAN_POINT('Ctrl Pts',(30.4349407351366,3.85593568953959,331.946978051072));
#27752=CARTESIAN_POINT('Ctrl Pts',(30.4271936567587,3.77077246687283,331.839417766472));
#27753=CARTESIAN_POINT('Ctrl Pts',(30.4194465783808,3.68108368870038,331.735396305966));
#27754=CARTESIAN_POINT('Ctrl Pts',(30.411699500003,3.58720318655211,331.635307389836));
#27755=CARTESIAN_POINT('Ctrl Pts',(30.4039523566972,3.49332189759481,331.535217634865));
#27756=CARTESIAN_POINT('Ctrl Pts',(30.3962052133914,3.39524908199738,331.439060775098));
#27757=CARTESIAN_POINT('Ctrl Pts',(30.3884580700856,3.2933565835326,331.347194848311));
#27758=CARTESIAN_POINT('Ctrl Pts',(30.3807091850575,3.19144117747106,331.255308268114));
#27759=CARTESIAN_POINT('Ctrl Pts',(30.3729603000294,3.08570466998124,331.167714802213));
#27760=CARTESIAN_POINT('Ctrl Pts',(30.3652114150013,2.97655292299249,331.08473299006));
#27761=CARTESIAN_POINT('Ctrl Pts',(30.3574543052266,2.86728532121158,331.001663100154));
#27762=CARTESIAN_POINT('Ctrl Pts',(30.3496971954519,2.75459555036754,330.923214878864));
#27763=CARTESIAN_POINT('Ctrl Pts',(30.3419400856772,2.63891992426349,330.84966450804));
#27764=CARTESIAN_POINT('Ctrl Pts',(30.334178830751,2.52318248480367,330.776074834249));
#27765=CARTESIAN_POINT('Ctrl Pts',(30.3264175758248,2.40445634897829,330.707388421677));
#27766=CARTESIAN_POINT('Ctrl Pts',(30.3186563208987,2.28320262771825,330.643835537623));
#27767=CARTESIAN_POINT('Ctrl Pts',(30.310882650494,2.16175494002051,330.580180989665));
#27768=CARTESIAN_POINT('Ctrl Pts',(30.3031089800893,2.0377719408323,330.521676547071));
#27769=CARTESIAN_POINT('Ctrl Pts',(30.2953353096846,1.91173573428443,330.468504712045));
#27770=CARTESIAN_POINT('Ctrl Pts',(30.2879235055076,1.79156654347443,330.417808038732));
#27771=CARTESIAN_POINT('Ctrl Pts',(30.2805117013306,1.66953126652681,330.371958781094));
#27772=CARTESIAN_POINT('Ctrl Pts',(30.2730998971535,1.54605893725225,330.331072411673));
#27773=CARTESIAN_POINT('Ctrl Pts',(30.2653248183751,1.41653486131422,330.288182079492));
#27774=CARTESIAN_POINT('Ctrl Pts',(30.2575497395966,1.28501998274813,330.250617886979));
#27775=CARTESIAN_POINT('Ctrl Pts',(30.2497746608182,1.15199174219043,330.218567360254));
#27776=CARTESIAN_POINT('Ctrl Pts',(30.2420091497692,1.01912720135174,330.186556273744));
#27777=CARTESIAN_POINT('Ctrl Pts',(30.2342436387202,0.884753380309309,330.160045443661));
#27778=CARTESIAN_POINT('Ctrl Pts',(30.2264781276712,0.749365239921871,330.139173444804));
#27779=CARTESIAN_POINT('Ctrl Pts',(30.218720316149,0.614111337269706,330.118322140595));
#27780=CARTESIAN_POINT('Ctrl Pts',(30.2109625046267,0.477845500495644,330.10309860054));
#27781=CARTESIAN_POINT('Ctrl Pts',(30.2032046931045,0.341074969304791,330.093590831594));
#27782=CARTESIAN_POINT('Ctrl Pts',(30.1954527195815,0.204407362275902,330.084090217546));
#27783=CARTESIAN_POINT('Ctrl Pts',(30.1877007460585,0.0672362051638616,
330.080296840078));
#27784=CARTESIAN_POINT('Ctrl Pts',(30.1799487725355,-0.0699243687591812,
330.082247093931));
#27785=CARTESIAN_POINT('Ctrl Pts',(30.1722000819779,-0.207026855097548,
330.084196521849));
#27786=CARTESIAN_POINT('Ctrl Pts',(30.1644513914202,-0.344118377139885,
330.091884737608));
#27787=CARTESIAN_POINT('Ctrl Pts',(30.1567027008626,-0.480683235067083,
330.105296056959));
#27788=CARTESIAN_POINT('Ctrl Pts',(30.1489556224848,-0.617219679534977,
330.118704585972));
#27789=CARTESIAN_POINT('Ctrl Pts',(30.1412085441069,-0.753229289085119,
330.137833811933));
#27790=CARTESIAN_POINT('Ctrl Pts',(30.1334614657291,-0.888200320536573,
330.162616073424));
#27791=CARTESIAN_POINT('Ctrl Pts',(30.1257143224233,-1.02317248317527,330.187398542613));
#27792=CARTESIAN_POINT('Ctrl Pts',(30.1179671791175,-1.15710566590641,330.217834071242));
#27793=CARTESIAN_POINT('Ctrl Pts',(30.1102200358117,-1.28949756112466,330.253803722732));
#27794=CARTESIAN_POINT('Ctrl Pts',(30.1024711507836,-1.42191922085154,330.289781460963));
#27795=CARTESIAN_POINT('Ctrl Pts',(30.0947222657555,-1.55279852641434,330.33129569539));
#27796=CARTESIAN_POINT('Ctrl Pts',(30.0869733807274,-1.68164797601495,330.378177508032));
#27797=CARTESIAN_POINT('Ctrl Pts',(30.0792162709527,-1.81063418775281,330.425109081514));
#27798=CARTESIAN_POINT('Ctrl Pts',(30.071459161178,-1.93758587179635,330.477419480049));
#27799=CARTESIAN_POINT('Ctrl Pts',(30.0637020514033,-2.06203466650152,330.534891255899));
#27800=CARTESIAN_POINT('Ctrl Pts',(30.0559407964771,-2.18654996266339,330.592393742828));
#27801=CARTESIAN_POINT('Ctrl Pts',(30.0481795415509,-2.30855935695502,330.655062924287));
#27802=CARTESIAN_POINT('Ctrl Pts',(30.0404182866247,-2.42761967910912,330.722635653103));
#27803=CARTESIAN_POINT('Ctrl Pts',(30.0326446162201,-2.54687045897701,330.790316476264));
#27804=CARTESIAN_POINT('Ctrl Pts',(30.0248709458154,-2.66316240789581,330.862916314471));
#27805=CARTESIAN_POINT('Ctrl Pts',(30.0170972754107,-2.77608116165939,330.94012851849));
#27806=CARTESIAN_POINT('Ctrl Pts',(30.0096854712336,-2.8837435202689,331.013746475836));
#27807=CARTESIAN_POINT('Ctrl Pts',(30.0022736670566,-2.98833942990736,331.091556879592));
#27808=CARTESIAN_POINT('Ctrl Pts',(29.9948618628795,-3.08953961243817,331.173261434893));
#27809=CARTESIAN_POINT('Ctrl Pts',(29.9871879224333,-3.1943189826596,331.25785566817));
#27810=CARTESIAN_POINT('Ctrl Pts',(29.9795139819871,-3.29580784769039,331.346907308451));
#27811=CARTESIAN_POINT('Ctrl Pts',(29.971840041541,-3.39359577220477,331.440127699288));
#27812=CARTESIAN_POINT('Ctrl Pts',(29.9641755913701,-3.49126276350013,331.533232805524));
#27813=CARTESIAN_POINT('Ctrl Pts',(29.9565111411992,-3.58523762853864,331.630496135086));
#27814=CARTESIAN_POINT('Ctrl Pts',(29.9488466910283,-3.67514112279571,331.731587420469));
#27815=CARTESIAN_POINT('Ctrl Pts',(29.941189771001,-3.76495628896586,331.832579386021));
#27816=CARTESIAN_POINT('Ctrl Pts',(29.9335328509736,-3.8507077755645,331.93739152815));
#27817=CARTESIAN_POINT('Ctrl Pts',(29.9258759309463,-3.93205187648206,332.045655554416));
#27818=CARTESIAN_POINT('Ctrl Pts',(29.9182246515771,-4.01333605327071,332.153839825328));
#27819=CARTESIAN_POINT('Ctrl Pts',(29.910573372208,-4.09021906416721,332.265470600495));
#27820=CARTESIAN_POINT('Ctrl Pts',(29.9029220928388,-4.16239667494011,332.380145617988));
#27821=CARTESIAN_POINT('Ctrl Pts',(29.895273816448,-4.23454595740404,332.494775627766));
#27822=CARTESIAN_POINT('Ctrl Pts',(29.8876255400571,-4.30199329779169,332.612447164746));
#27823=CARTESIAN_POINT('Ctrl Pts',(29.8799772636663,-4.36447731831841,332.732728335557));
#27824=CARTESIAN_POINT('Ctrl Pts',(29.8723302316669,-4.42695117255783,332.852989936358));
#27825=CARTESIAN_POINT('Ctrl Pts',(29.8646831996675,-4.48446312793866,332.975859969888));
#27826=CARTESIAN_POINT('Ctrl Pts',(29.857036167668,-4.53679764761379,333.100881739568));
#27827=CARTESIAN_POINT('Ctrl Pts',(29.84938862272,-4.58913567779022,333.225911895474));
#27828=CARTESIAN_POINT('Ctrl Pts',(29.841741077772,-4.63629542740628,333.35309370338));
#27829=CARTESIAN_POINT('Ctrl Pts',(29.834093532824,-4.67810962638648,333.481950795919));
#27830=CARTESIAN_POINT('Ctrl Pts',(29.8264396786577,-4.71995832204658,333.610914195454));
#27831=CARTESIAN_POINT('Ctrl Pts',(29.8187858244914,-4.75645253434975,333.741555257285));
#27832=CARTESIAN_POINT('Ctrl Pts',(29.8111319703251,-4.78747492394016,333.873382533801));
#27833=CARTESIAN_POINT('Ctrl Pts',(29.8034748858929,-4.81851040635478,334.005265447275));
#27834=CARTESIAN_POINT('Ctrl Pts',(29.7958178014607,-4.844069390303,334.138335178013));
#27835=CARTESIAN_POINT('Ctrl Pts',(29.7881607170285,-4.86408598944587,334.272091661144));
#27836=CARTESIAN_POINT('Ctrl Pts',(29.7804931283228,-4.88413004810485,334.406031636399));
#27837=CARTESIAN_POINT('Ctrl Pts',(29.772825539617,-4.89861649109298,334.540659846392));
#27838=CARTESIAN_POINT('Ctrl Pts',(29.7651579509112,-4.90753143194119,334.675472178374));
#27839=CARTESIAN_POINT('Ctrl Pts',(29.7589507167834,-4.91474844985958,334.784608406208));
#27840=CARTESIAN_POINT('Ctrl Pts',(29.7527434826556,-4.91831513988253,334.893865175375));
#27841=CARTESIAN_POINT('Ctrl Pts',(29.7465362485277,-4.91824909912948,335.002976812401));
#27842=CARTESIAN_POINT('',(33.2465372519956,-4.91612741639346,334.995890487429));
#27843=CARTESIAN_POINT('Ctrl Pts',(33.2465362484901,-4.91824829644928,334.995906471729));
#27844=CARTESIAN_POINT('Ctrl Pts',(33.2385755814652,-4.91836558057476,335.136819740692));
#27845=CARTESIAN_POINT('Ctrl Pts',(33.2306149144403,-4.91242204025201,335.27782646653));
#27846=CARTESIAN_POINT('Ctrl Pts',(33.2226542474154,-4.90042391361396,335.418364111009));
#27847=CARTESIAN_POINT('Ctrl Pts',(33.214938036397,-4.88879422521277,335.554586128265));
#27848=CARTESIAN_POINT('Ctrl Pts',(33.2072218253785,-4.87147638372207,335.690367031991));
#27849=CARTESIAN_POINT('Ctrl Pts',(33.1995056143601,-4.84852893196693,335.825197102746));
#27850=CARTESIAN_POINT('Ctrl Pts',(33.1917896841848,-4.82558231541894,335.960022266156));
#27851=CARTESIAN_POINT('Ctrl Pts',(33.1840737540096,-4.79700656195118,336.093896276925));
#27852=CARTESIAN_POINT('Ctrl Pts',(33.1763578238343,-4.76291165079966,336.226317931524));
#27853=CARTESIAN_POINT('Ctrl Pts',(33.1686404726742,-4.72881046064511,336.358763973222));
#27854=CARTESIAN_POINT('Ctrl Pts',(33.1609231215142,-4.6891881887503,336.489756745004));
#27855=CARTESIAN_POINT('Ctrl Pts',(33.1532057703542,-4.64420504520035,336.618808994488));
#27856=CARTESIAN_POINT('Ctrl Pts',(33.1454852957562,-4.59920369565548,336.747913475195));
#27857=CARTESIAN_POINT('Ctrl Pts',(33.1377648211582,-4.54883728704591,336.875075499219));
#27858=CARTESIAN_POINT('Ctrl Pts',(33.1300443465603,-4.49331446627497,336.999827034937));
#27859=CARTESIAN_POINT('Ctrl Pts',(33.1223148311214,-4.43772662709326,337.124724657371));
#27860=CARTESIAN_POINT('Ctrl Pts',(33.1145853156826,-4.37697048298475,337.247205797077));
#27861=CARTESIAN_POINT('Ctrl Pts',(33.1068558002437,-4.31130118631532,337.366825963897));
#27862=CARTESIAN_POINT('Ctrl Pts',(33.099120859815,-4.24558579939964,337.486530086587));
#27863=CARTESIAN_POINT('Ctrl Pts',(33.0913859193863,-4.1749505960538,337.603368901739));
#27864=CARTESIAN_POINT('Ctrl Pts',(33.0836509789576,-4.09969386809841,337.716927170606));
#27865=CARTESIAN_POINT('Ctrl Pts',(33.0759049469835,-4.02432922549006,337.830648276757));
#27866=CARTESIAN_POINT('Ctrl Pts',(33.0681589150093,-3.94433006251908,337.941079131096));
#27867=CARTESIAN_POINT('Ctrl Pts',(33.0604128830352,-3.86003489097701,338.047837545366));
#27868=CARTESIAN_POINT('Ctrl Pts',(33.0587686686544,-3.84214194478911,338.070498660192));
#27869=CARTESIAN_POINT('Ctrl Pts',(33.0571244542736,-3.82405556599331,338.092994440948));
#27870=CARTESIAN_POINT('Ctrl Pts',(33.0554802398928,-3.80577919883156,338.115321452473));
#27871=CARTESIAN_POINT('Ctrl Pts',(33.0477051611144,-3.71935482733553,338.220900308566));
#27872=CARTESIAN_POINT('Ctrl Pts',(33.0399300823359,-3.62839715136282,338.323046933694));
#27873=CARTESIAN_POINT('Ctrl Pts',(33.0321550035575,-3.53320898375705,338.421347298887));
#27874=CARTESIAN_POINT('Ctrl Pts',(33.0243894925085,-3.43813795125148,338.519526699222));
#27875=CARTESIAN_POINT('Ctrl Pts',(33.0166239814595,-3.33884705464954,338.613868978955));
#27876=CARTESIAN_POINT('Ctrl Pts',(33.0088584704104,-3.23568011531128,338.7039920699));
#27877=CARTESIAN_POINT('Ctrl Pts',(33.0011006588883,-3.13261546629395,338.794025803537));
#27878=CARTESIAN_POINT('Ctrl Pts',(32.9933428473661,-3.02568271501763,338.879848417969));
#27879=CARTESIAN_POINT('Ctrl Pts',(32.9855850358439,-2.9152631303013,338.961113977609));
#27880=CARTESIAN_POINT('Ctrl Pts',(32.9778330623208,-2.80492663982333,339.042318382338));
#27881=CARTESIAN_POINT('Ctrl Pts',(32.9700810887978,-2.691108852294,339.11897232743));
#27882=CARTESIAN_POINT('Ctrl Pts',(32.9623291152747,-2.57422449503257,339.190769775551));
#27883=CARTESIAN_POINT('Ctrl Pts',(32.9545804247171,-2.45738963836647,339.26253681741));
#27884=CARTESIAN_POINT('Ctrl Pts',(32.9468317341594,-2.33749112734454,339.32945124883));
#27885=CARTESIAN_POINT('Ctrl Pts',(32.9390830436018,-2.21497289874997,339.391250177376));
#27886=CARTESIAN_POINT('Ctrl Pts',(32.931335965224,-2.09248016109599,339.453036248139));
#27887=CARTESIAN_POINT('Ctrl Pts',(32.9235888868462,-1.96736913879282,339.50970875712));
#27888=CARTESIAN_POINT('Ctrl Pts',(32.9158418084683,-1.84010825891691,339.561050828259));
#27889=CARTESIAN_POINT('Ctrl Pts',(32.9080946651625,-1.71284631247242,339.612393329695));
#27890=CARTESIAN_POINT('Ctrl Pts',(32.9003475218567,-1.58343483500336,339.658405157943));
#27891=CARTESIAN_POINT('Ctrl Pts',(32.8926003785509,-1.4523617406965,339.698917794201));
#27892=CARTESIAN_POINT('Ctrl Pts',(32.8848514935228,-1.32125917837545,339.739439538561));
#27893=CARTESIAN_POINT('Ctrl Pts',(32.8771026084947,-1.18849462923059,339.77445951536));
#27894=CARTESIAN_POINT('Ctrl Pts',(32.8693537234666,-1.05457026632765,339.803859345971));
#27895=CARTESIAN_POINT('Ctrl Pts',(32.8615966136919,-0.920503754722047,
339.833290381867));
#27896=CARTESIAN_POINT('Ctrl Pts',(32.8538395039171,-0.785275352630049,
339.857089271423));
#27897=CARTESIAN_POINT('Ctrl Pts',(32.8460823941423,-0.649397054085376,
339.875188871074));
#27898=CARTESIAN_POINT('Ctrl Pts',(32.8383211392162,-0.5134461465226,339.893298142572));
#27899=CARTESIAN_POINT('Ctrl Pts',(32.8305598842901,-0.376845039588008,
339.905702020367));
#27900=CARTESIAN_POINT('Ctrl Pts',(32.8227986293639,-0.240108922136284,
339.91238544579));
#27901=CARTESIAN_POINT('Ctrl Pts',(32.8150249589592,-0.103154071458833,
339.919079562516));
#27902=CARTESIAN_POINT('Ctrl Pts',(32.8072512885546,0.0339358302430315,
339.920034938019));
#27903=CARTESIAN_POINT('Ctrl Pts',(32.7994776181499,0.170646628716568,339.915288678258));
#27904=CARTESIAN_POINT('Ctrl Pts',(32.7920658139729,0.300993506628775,339.91076335803));
#27905=CARTESIAN_POINT('Ctrl Pts',(32.7846540097959,0.430995494545105,339.90105530039));
#27906=CARTESIAN_POINT('Ctrl Pts',(32.7772422056189,0.560214771800575,339.886240116077));
#27907=CARTESIAN_POINT('Ctrl Pts',(32.7694671268405,0.695767470760528,339.870698795448));
#27908=CARTESIAN_POINT('Ctrl Pts',(32.761692048062,0.830887164652608,339.849487945254));
#27909=CARTESIAN_POINT('Ctrl Pts',(32.7539169692836,0.965061818276978,339.822638152444));
#27910=CARTESIAN_POINT('Ctrl Pts',(32.7461514582346,1.09907136144809,339.795821400012));
#27911=CARTESIAN_POINT('Ctrl Pts',(32.7383859471855,1.23213779864149,339.763379587704));
#27912=CARTESIAN_POINT('Ctrl Pts',(32.7306204361365,1.36375377910245,339.725395083216));
#27913=CARTESIAN_POINT('Ctrl Pts',(32.7228626246143,1.4952392619355,339.687448240475));
#27914=CARTESIAN_POINT('Ctrl Pts',(32.7151048130922,1.62527677687213,339.643969749787));
#27915=CARTESIAN_POINT('Ctrl Pts',(32.70734700157,1.75336909286239,339.595093022638));
#27916=CARTESIAN_POINT('Ctrl Pts',(32.6995950280469,1.88136501532299,339.546253076776));
#27917=CARTESIAN_POINT('Ctrl Pts',(32.6918430545239,2.00741828878591,339.492023119139));
#27918=CARTESIAN_POINT('Ctrl Pts',(32.6840910810008,2.13104712717919,339.432586288415));
#27919=CARTESIAN_POINT('Ctrl Pts',(32.6763423904432,2.25462360868584,339.373174629224));
#27920=CARTESIAN_POINT('Ctrl Pts',(32.6685936998856,2.37577734571228,339.308560651773));
#27921=CARTESIAN_POINT('Ctrl Pts',(32.6608450093279,2.49404702673606,339.238975405794));
#27922=CARTESIAN_POINT('Ctrl Pts',(32.6530979309501,2.61229210076489,339.169404637607));
#27923=CARTESIAN_POINT('Ctrl Pts',(32.6453508525723,2.72765397565889,339.094864856303));
#27924=CARTESIAN_POINT('Ctrl Pts',(32.6376037741945,2.83969678294388,339.015632608125));
#27925=CARTESIAN_POINT('Ctrl Pts',(32.6298566308887,2.9517405292552,338.936399695905));
#27926=CARTESIAN_POINT('Ctrl Pts',(32.6221094875828,3.06046483333505,338.852474464051));
#27927=CARTESIAN_POINT('Ctrl Pts',(32.6143623442771,3.16546394576596,338.764176014821));
#27928=CARTESIAN_POINT('Ctrl Pts',(32.606613459249,3.27048666422669,338.675857714225));
#27929=CARTESIAN_POINT('Ctrl Pts',(32.5988645742209,3.37178222540607,338.583164491334));
#27930=CARTESIAN_POINT('Ctrl Pts',(32.5911156891928,3.46897932753056,338.486454572724));
#27931=CARTESIAN_POINT('Ctrl Pts',(32.583358579418,3.56627959566361,338.389642005207));
#27932=CARTESIAN_POINT('Ctrl Pts',(32.5756014696433,3.65947243739439,338.288804501635));
#27933=CARTESIAN_POINT('Ctrl Pts',(32.5678443598686,3.7482243209166,338.184336273478));
#27934=CARTESIAN_POINT('Ctrl Pts',(32.5600831049424,3.83702363060768,338.079812220841));
#27935=CARTESIAN_POINT('Ctrl Pts',(32.5523218500163,3.92137701320233,337.971653885771));
#27936=CARTESIAN_POINT('Ctrl Pts',(32.5445605950901,4.00099300729565,337.86028635246));
#27937=CARTESIAN_POINT('Ctrl Pts',(32.5367869246854,4.08073636103262,337.748740667391));
#27938=CARTESIAN_POINT('Ctrl Pts',(32.5290132542807,4.15572696870276,337.633975852869));
#27939=CARTESIAN_POINT('Ctrl Pts',(32.5212395838761,4.22571779513056,337.516444352339));
#27940=CARTESIAN_POINT('Ctrl Pts',(32.513827779699,4.29245053174894,337.404383971435));
#27941=CARTESIAN_POINT('Ctrl Pts',(32.506415975522,4.35463835414161,337.289808939287));
#27942=CARTESIAN_POINT('Ctrl Pts',(32.4990041713449,4.41210791510817,337.173128345943));
#27943=CARTESIAN_POINT('Ctrl Pts',(32.4912290925665,4.47239423045099,337.050728889144));
#27944=CARTESIAN_POINT('Ctrl Pts',(32.4834540137881,4.52767859354105,336.92562544778));
#27945=CARTESIAN_POINT('Ctrl Pts',(32.4756789350097,4.57770963396754,336.798265155527));
#27946=CARTESIAN_POINT('Ctrl Pts',(32.4679134239606,4.62767910801365,336.67106158822));
#27947=CARTESIAN_POINT('Ctrl Pts',(32.4601479129116,4.6724079804435,336.541607056186));
#27948=CARTESIAN_POINT('Ctrl Pts',(32.4523824018626,4.71169095940682,336.410372775384));
#27949=CARTESIAN_POINT('Ctrl Pts',(32.4446245903404,4.7509349891821,336.279268613754));
#27950=CARTESIAN_POINT('Ctrl Pts',(32.4368667788182,4.78474375967213,336.146388587108));
#27951=CARTESIAN_POINT('Ctrl Pts',(32.4291089672961,4.8129603791914,336.012223024256));
#27952=CARTESIAN_POINT('Ctrl Pts',(32.4213569937731,4.84115576480965,335.878158425245));
#27953=CARTESIAN_POINT('Ctrl Pts',(32.4136050202501,4.86376729569296,335.74281059657));
#27954=CARTESIAN_POINT('Ctrl Pts',(32.4058530467271,4.88068825498377,335.60668378927));
#27955=CARTESIAN_POINT('Ctrl Pts',(32.3981043561695,4.89760204823829,335.470614631755));
#27956=CARTESIAN_POINT('Ctrl Pts',(32.3903556656119,4.90883001502641,335.33376753884));
#27957=CARTESIAN_POINT('Ctrl Pts',(32.3826069750543,4.91431680786163,335.196655471494));
#27958=CARTESIAN_POINT('Ctrl Pts',(32.3748598966765,4.91980245912377,335.05957193146));
#27959=CARTESIAN_POINT('Ctrl Pts',(32.3671128182986,4.91954929675717,334.922223916969));
#27960=CARTESIAN_POINT('Ctrl Pts',(32.3593657399208,4.91355400095527,334.78512761416));
#27961=CARTESIAN_POINT('Ctrl Pts',(32.351618596615,4.90755865490702,334.648030162352));
#27962=CARTESIAN_POINT('Ctrl Pts',(32.3438714533092,4.89582109651214,334.511184816935));
#27963=CARTESIAN_POINT('Ctrl Pts',(32.3361243100034,4.8783900913741,334.375105465792));
#27964=CARTESIAN_POINT('Ctrl Pts',(32.3283754249753,4.86095516737602,334.238995521121));
#27965=CARTESIAN_POINT('Ctrl Pts',(32.3206265399472,4.83782429921578,334.103652301037));
#27966=CARTESIAN_POINT('Ctrl Pts',(32.3128776549191,4.80909779456918,333.969581898077));
#27967=CARTESIAN_POINT('Ctrl Pts',(32.3051205451444,4.78034079931375,333.835369191407));
#27968=CARTESIAN_POINT('Ctrl Pts',(32.2973634353697,4.74597638535125,333.702432383376));
#27969=CARTESIAN_POINT('Ctrl Pts',(32.289606325595,4.7061555603185,333.571265278443));
#27970=CARTESIAN_POINT('Ctrl Pts',(32.2818450706688,4.6663134563101,333.440028082003));
#27971=CARTESIAN_POINT('Ctrl Pts',(32.2740838157427,4.62100926041166,333.310562841749));
#27972=CARTESIAN_POINT('Ctrl Pts',(32.2663225608165,4.57044270849739,333.183344691241));
#27973=CARTESIAN_POINT('Ctrl Pts',(32.2585488904119,4.51979526657965,333.055923033153));
#27974=CARTESIAN_POINT('Ctrl Pts',(32.2507752200072,4.46386880641896,332.930756004967));
#27975=CARTESIAN_POINT('Ctrl Pts',(32.2430015496026,4.40291011245137,332.808296186942));
#27976=CARTESIAN_POINT('Ctrl Pts',(32.2355897454254,4.34478906035313,332.691536902907));
#27977=CARTESIAN_POINT('Ctrl Pts',(32.2281779412482,4.28209387050131,332.577238712127));
#27978=CARTESIAN_POINT('Ctrl Pts',(32.2207661370711,4.21507474732732,332.465768768059));
#27979=CARTESIAN_POINT('Ctrl Pts',(32.2129910582926,4.14477081728747,332.348835349982));
#27980=CARTESIAN_POINT('Ctrl Pts',(32.2052159795142,4.0694862055636,332.234644899063));
#27981=CARTESIAN_POINT('Ctrl Pts',(32.1974409007357,3.98946088544972,332.123650767732));
#27982=CARTESIAN_POINT('Ctrl Pts',(32.1896753896867,3.909534041587,332.012793221746));
#27983=CARTESIAN_POINT('Ctrl Pts',(32.1819098786377,3.82487832322155,331.905124483288));
#27984=CARTESIAN_POINT('Ctrl Pts',(32.1741443675887,3.73577889070845,331.801072188649));
#27985=CARTESIAN_POINT('Ctrl Pts',(32.1663865560664,3.6467678005419,331.697123062162));
#27986=CARTESIAN_POINT('Ctrl Pts',(32.1586287445442,3.55332201692302,331.596783538706));
#27987=CARTESIAN_POINT('Ctrl Pts',(32.150870933022,3.45576896471481,331.500450896899));
#27988=CARTESIAN_POINT('Ctrl Pts',(32.143118959499,3.35828932427225,331.40419074846));
#27989=CARTESIAN_POINT('Ctrl Pts',(32.1353669859759,3.25670884443015,331.311931753392));
#27990=CARTESIAN_POINT('Ctrl Pts',(32.1276150124529,3.15139381003039,331.224036531347));
#27991=CARTESIAN_POINT('Ctrl Pts',(32.1198663218953,3.04612337661021,331.136178532981));
#27992=CARTESIAN_POINT('Ctrl Pts',(32.1121176313377,2.93712183376301,331.05268088191));
#27993=CARTESIAN_POINT('Ctrl Pts',(32.1043689407801,2.82479058960962,330.97386771363));
#27994=CARTESIAN_POINT('Ctrl Pts',(32.0966218624023,2.7124827169098,330.895070943088));
#27995=CARTESIAN_POINT('Ctrl Pts',(32.0888747840245,2.59684684064964,330.820956941054));
#27996=CARTESIAN_POINT('Ctrl Pts',(32.0811277056466,2.47831523622769,330.751807837164));
#27997=CARTESIAN_POINT('Ctrl Pts',(32.0733805623408,2.35978263839706,330.682658153738));
#27998=CARTESIAN_POINT('Ctrl Pts',(32.065633419035,2.23835460162027,330.618473648413));
#27999=CARTESIAN_POINT('Ctrl Pts',(32.0578862757292,2.11448965504715,330.559491407372));
#28000=CARTESIAN_POINT('Ctrl Pts',(32.0501373907011,1.99059686100465,330.500495905872));
#28001=CARTESIAN_POINT('Ctrl Pts',(32.0423885056731,1.86426641980479,330.446705164004));
#28002=CARTESIAN_POINT('Ctrl Pts',(32.034639620645,1.73597819769921,330.398308706615));
#28003=CARTESIAN_POINT('Ctrl Pts',(32.0268825108703,1.6075538091487,330.349860880726));
#28004=CARTESIAN_POINT('Ctrl Pts',(32.0191254010956,1.47716785496841,330.306818914822));
#28005=CARTESIAN_POINT('Ctrl Pts',(32.0113682913208,1.34531730475887,330.269323049286));
#28006=CARTESIAN_POINT('Ctrl Pts',(32.0036070363947,1.2133962978306,330.231807147158));
#28007=CARTESIAN_POINT('Ctrl Pts',(31.9958457814685,1.0800095153258,330.199843341796));
#28008=CARTESIAN_POINT('Ctrl Pts',(31.9880845265423,0.945664595734111,330.173520793075));
#28009=CARTESIAN_POINT('Ctrl Pts',(31.9803108561376,0.811104768054161,330.147156136855));
#28010=CARTESIAN_POINT('Ctrl Pts',(31.9725371857329,0.675584127078492,330.126450829309));
#28011=CARTESIAN_POINT('Ctrl Pts',(31.9647635153282,0.539616806420292,330.111442261287));
#28012=CARTESIAN_POINT('Ctrl Pts',(31.9573517111512,0.40997879725149,330.097132345718));
#28013=CARTESIAN_POINT('Ctrl Pts',(31.9499399069741,0.279935045503705,330.088000758948));
#28014=CARTESIAN_POINT('Ctrl Pts',(31.9425281027971,0.149929698326431,330.084035786536));
#28015=CARTESIAN_POINT('Ctrl Pts',(31.9347530240187,0.0135524018171826,
330.079876479015));
#28016=CARTESIAN_POINT('Ctrl Pts',(31.9269779452402,-0.12321360774063,330.081389909902));
#28017=CARTESIAN_POINT('Ctrl Pts',(31.9192028664618,-0.259857233298094,
330.088619615546));
#28018=CARTESIAN_POINT('Ctrl Pts',(31.9114373554128,-0.396332710175151,
330.095840424577));
#28019=CARTESIAN_POINT('Ctrl Pts',(31.9036718443638,-0.532685716108326,
330.10876349179));
#28020=CARTESIAN_POINT('Ctrl Pts',(31.8959063333147,-0.668402325986071,
330.127380438294));
#28021=CARTESIAN_POINT('Ctrl Pts',(31.8881485217925,-0.803984372450086,
330.145978926042));
#28022=CARTESIAN_POINT('Ctrl Pts',(31.8803907102703,-0.938930893808257,
330.170260005443));
#28023=CARTESIAN_POINT('Ctrl Pts',(31.8726328987481,-1.07273062161303,330.2001633282));
#28024=CARTESIAN_POINT('Ctrl Pts',(31.8648809252251,-1.20642966088014,330.230044147759));
#28025=CARTESIAN_POINT('Ctrl Pts',(31.857128951702,-1.33898324442268,330.265538704331));
#28026=CARTESIAN_POINT('Ctrl Pts',(31.849376978179,-1.46988821989237,330.306535215481));
#28027=CARTESIAN_POINT('Ctrl Pts',(31.8416282876214,-1.60073775702633,330.347514364583));
#28028=CARTESIAN_POINT('Ctrl Pts',(31.8338795970637,-1.72993970249786,330.393990717321));
#28029=CARTESIAN_POINT('Ctrl Pts',(31.8261309065061,-1.85700425888646,330.445802129356));
#28030=CARTESIAN_POINT('Ctrl Pts',(31.8183838281283,-1.98404237843301,330.497602761595));
#28031=CARTESIAN_POINT('Ctrl Pts',(31.8106367497505,-2.10894363172539,330.554736097764));
#28032=CARTESIAN_POINT('Ctrl Pts',(31.8028896713726,-2.23123684091283,330.616991304794));
#28033=CARTESIAN_POINT('Ctrl Pts',(31.7951425280668,-2.35353107503499,330.679247033582));
#28034=CARTESIAN_POINT('Ctrl Pts',(31.787395384761,-2.47321687311857,330.746624541524));
#28035=CARTESIAN_POINT('Ctrl Pts',(31.7796482414552,-2.58984672790028,330.818866542613));
#28036=CARTESIAN_POINT('Ctrl Pts',(31.7718993564271,-2.70650280354979,330.891124785237));
#28037=CARTESIAN_POINT('Ctrl Pts',(31.764150471399,-2.82010123653514,330.968249491448));
#28038=CARTESIAN_POINT('Ctrl Pts',(31.7564015863709,-2.93022296820521,331.049939694245));
#28039=CARTESIAN_POINT('Ctrl Pts',(31.7486444765962,-3.04046158421874,331.131716603867));
#28040=CARTESIAN_POINT('Ctrl Pts',(31.7408873668215,-3.14721581295896,331.218068456901));
#28041=CARTESIAN_POINT('Ctrl Pts',(31.7331302570468,-3.2500987845288,331.308653233127));
#28042=CARTESIAN_POINT('Ctrl Pts',(31.7253690021206,-3.35303673346916,331.39928641496));
#28043=CARTESIAN_POINT('Ctrl Pts',(31.7176077471944,-3.45209902106075,331.494156756887));
#28044=CARTESIAN_POINT('Ctrl Pts',(31.7098464922682,-3.54693595854771,331.592885624394));
#28045=CARTESIAN_POINT('Ctrl Pts',(31.7020728218636,-3.64192460422749,331.691772425914));
#28046=CARTESIAN_POINT('Ctrl Pts',(31.6942991514589,-3.73267413407582,331.794529794133));
#28047=CARTESIAN_POINT('Ctrl Pts',(31.6865254810542,-3.81887487813061,331.900745617462));
#28048=CARTESIAN_POINT('Ctrl Pts',(31.6791136768772,-3.90106295681072,332.00201706866));
#28049=CARTESIAN_POINT('Ctrl Pts',(31.6717018727001,-3.97911603891936,332.106432008296));
#28050=CARTESIAN_POINT('Ctrl Pts',(31.664290068523,-4.0528036218724,332.213610604198));
#28051=CARTESIAN_POINT('Ctrl Pts',(31.6564069701454,-4.1311767752573,332.327604362707));
#28052=CARTESIAN_POINT('Ctrl Pts',(31.6485238717677,-4.2048548864954,332.44507877176));
#28053=CARTESIAN_POINT('Ctrl Pts',(31.6406407733901,-4.27351847197092,332.56561651907));
#28054=CARTESIAN_POINT('Ctrl Pts',(31.6327680418378,-4.34209176003261,332.685995750819));
#28055=CARTESIAN_POINT('Ctrl Pts',(31.6248953102855,-4.40566346273056,332.809429978934));
#28056=CARTESIAN_POINT('Ctrl Pts',(31.6170225787332,-4.46395620642664,332.935471470382));
#28057=CARTESIAN_POINT('Ctrl Pts',(31.609158664089,-4.5221836663311,333.061371804186));
#28058=CARTESIAN_POINT('Ctrl Pts',(31.6012947494448,-4.57514377911361,333.189873249273));
#28059=CARTESIAN_POINT('Ctrl Pts',(31.5934308348006,-4.62260422957602,333.320502099077));
#28060=CARTESIAN_POINT('Ctrl Pts',(31.5853562859414,-4.67133590374573,333.454629830351));
#28061=CARTESIAN_POINT('Ctrl Pts',(31.5772817370822,-4.71426893629634,333.591000198089));
#28062=CARTESIAN_POINT('Ctrl Pts',(31.5692071882229,-4.75120345817438,333.729075627139));
#28063=CARTESIAN_POINT('Ctrl Pts',(31.561357229452,-4.78711066228243,333.86331054778));
#28064=CARTESIAN_POINT('Ctrl Pts',(31.553507270681,-4.81734850360566,333.999156548042));
#28065=CARTESIAN_POINT('Ctrl Pts',(31.54565731191,-4.84178310468622,334.136102187944));
#28066=CARTESIAN_POINT('Ctrl Pts',(31.5374704680067,-4.86726632959515,334.27892492241));
#28067=CARTESIAN_POINT('Ctrl Pts',(31.5292836241034,-4.88643701749181,334.422943374421));
#28068=CARTESIAN_POINT('Ctrl Pts',(31.5210967802001,-4.89920217817375,334.567563785192));
#28069=CARTESIAN_POINT('Ctrl Pts',(31.5129099362968,-4.91196733885568,334.712184195962));
#28070=CARTESIAN_POINT('Ctrl Pts',(31.5047230923934,-4.91832691382983,334.857406103153));
#28071=CARTESIAN_POINT('Ctrl Pts',(31.4965362484901,-4.91824929754544,335.002628629631));
#28072=CARTESIAN_POINT('',(34.9965357556323,-4.92245962640078,334.9992848849));
#28073=CARTESIAN_POINT('Ctrl Pts',(34.9965353149058,-4.92622403178934,334.999292078765));
#28074=CARTESIAN_POINT('Ctrl Pts',(34.905993025116,-4.92295145947301,336.59090228179));
#28075=CARTESIAN_POINT('Ctrl Pts',(34.7227047239016,-3.21855768239145,339.818862479759));
#28076=CARTESIAN_POINT('Ctrl Pts',(34.4466704112626,2.283209725273,340.34896272345));
#28077=CARTESIAN_POINT('Ctrl Pts',(34.1684323769887,5.73363266215494,335.97463088495));
#28078=CARTESIAN_POINT('Ctrl Pts',(33.8901943427146,3.92238553325728,330.70589466886));
#28079=CARTESIAN_POINT('Ctrl Pts',(33.6119563084407,-1.48837690519751,329.377795534267));
#28080=CARTESIAN_POINT('Ctrl Pts',(33.3974042091434,-4.60743999916255,332.332160351074));
#28081=CARTESIAN_POINT('Ctrl Pts',(33.2755981212709,-4.91847296868088,334.481873404345));
#28082=CARTESIAN_POINT('Ctrl Pts',(33.2465380448228,-4.9144517986456,334.995877858909));
#28083=CARTESIAN_POINT('',(36.7465362484456,-4.9182479594994,335.004480109374));
#28084=CARTESIAN_POINT('Ctrl Pts',(36.7465362484457,-4.9182479594994,335.004480109374));
#28085=CARTESIAN_POINT('Ctrl Pts',(36.7368046369555,-4.91809128867769,335.17647277404));
#28086=CARTESIAN_POINT('Ctrl Pts',(36.7270730254652,-4.90890910186633,335.348063028799));
#28087=CARTESIAN_POINT('Ctrl Pts',(36.717341413975,-4.89084924610496,335.518436798824));
#28088=CARTESIAN_POINT('Ctrl Pts',(36.7074286083814,-4.87245313160836,335.69198277959));
#28089=CARTESIAN_POINT('Ctrl Pts',(36.6975158027879,-4.844845702818,335.864266712581));
#28090=CARTESIAN_POINT('Ctrl Pts',(36.6876029971943,-4.80823161056874,336.034452435653));
#28091=CARTESIAN_POINT('Ctrl Pts',(36.6825935599475,-4.78972867557836,336.120455806946));
#28092=CARTESIAN_POINT('Ctrl Pts',(36.6775841227008,-4.76892638705445,336.205923705473));
#28093=CARTESIAN_POINT('Ctrl Pts',(36.672574685454,-4.74585574177114,336.290750301491));
#28094=CARTESIAN_POINT('Ctrl Pts',(36.6647996066755,-4.71004810995311,336.422408496624));
#28095=CARTESIAN_POINT('Ctrl Pts',(36.6570245278971,-4.66870110703505,336.552783560165));
#28096=CARTESIAN_POINT('Ctrl Pts',(36.6492494491186,-4.62192219533737,336.681373927105));
#28097=CARTESIAN_POINT('Ctrl Pts',(36.6414839380696,-4.57520084806862,336.809806055412));
#28098=CARTESIAN_POINT('Ctrl Pts',(36.6337184270205,-4.52306102422823,336.936457493079));
#28099=CARTESIAN_POINT('Ctrl Pts',(36.6259529159715,-4.46566066806993,337.060839115543));
#28100=CARTESIAN_POINT('Ctrl Pts',(36.6181951044492,-4.40831722453184,337.185097413267));
#28101=CARTESIAN_POINT('Ctrl Pts',(36.610437292927,-4.34572379120724,337.307090021847));
#28102=CARTESIAN_POINT('Ctrl Pts',(36.6026794814048,-4.27808724600464,337.426345519103));
#28103=CARTESIAN_POINT('Ctrl Pts',(36.5949275078817,-4.21050159944728,337.545511272815));
#28104=CARTESIAN_POINT('Ctrl Pts',(36.5871755343587,-4.13788058703176,337.661943676432));
#28105=CARTESIAN_POINT('Ctrl Pts',(36.5794235608356,-4.06047791563382,337.775194075943));
#28106=CARTESIAN_POINT('Ctrl Pts',(36.571674870278,-3.98310802431316,337.888396513843));
#28107=CARTESIAN_POINT('Ctrl Pts',(36.5639261797204,-3.90096072176034,337.998419305849));
#28108=CARTESIAN_POINT('Ctrl Pts',(36.5561774891627,-3.81433398987333,338.104841264251));
#28109=CARTESIAN_POINT('Ctrl Pts',(36.5484304107849,-3.72772528140129,338.211241080676));
#28110=CARTESIAN_POINT('Ctrl Pts',(36.540683332407,-3.63663924397457,338.314041250724));
#28111=CARTESIAN_POINT('Ctrl Pts',(36.5329362540292,-3.54141499825141,338.412852600488));
#28112=CARTESIAN_POINT('Ctrl Pts',(36.5251891107233,-3.44618995445762,338.511664778387));
#28113=CARTESIAN_POINT('Ctrl Pts',(36.5174419674175,-3.34682690442515,338.606487787871));
#28114=CARTESIAN_POINT('Ctrl Pts',(36.5096948241117,-3.24370249547495,338.696968647872));
#28115=CARTESIAN_POINT('Ctrl Pts',(36.5019459390836,-3.14055490196794,338.787469849892));
#28116=CARTESIAN_POINT('Ctrl Pts',(36.4941970540554,-3.03364456058375,338.873626702144));
#28117=CARTESIAN_POINT('Ctrl Pts',(36.4864481690273,-2.92338160002829,338.955126177901));
#28118=CARTESIAN_POINT('Ctrl Pts',(36.4786910592525,-2.81300160522727,339.036712158044));
#28119=CARTESIAN_POINT('Ctrl Pts',(36.4709339494777,-2.69926219763536,339.113630654111));
#28120=CARTESIAN_POINT('Ctrl Pts',(36.463176839703,-2.58260338275419,339.185611404549));
#28121=CARTESIAN_POINT('Ctrl Pts',(36.4554155847768,-2.46588222913245,339.257630619198));
#28122=CARTESIAN_POINT('Ctrl Pts',(36.4476543298506,-2.34623890048053,339.324706639573));
#28123=CARTESIAN_POINT('Ctrl Pts',(36.4398930749244,-2.22413757680755,339.386615449516));
#28124=CARTESIAN_POINT('Ctrl Pts',(36.4321194045197,-2.10184093080958,339.448623293379));
#28125=CARTESIAN_POINT('Ctrl Pts',(36.424345734115,-1.97707878841167,339.50544724709));
#28126=CARTESIAN_POINT('Ctrl Pts',(36.4165720637103,-1.85033567554691,339.556911338867));
#28127=CARTESIAN_POINT('Ctrl Pts',(36.4091602595336,-1.7294924850843,339.605979764788));
#28128=CARTESIAN_POINT('Ctrl Pts',(36.4017484553568,-1.60684887281296,339.650176004598));
#28129=CARTESIAN_POINT('Ctrl Pts',(36.3943366511801,-1.48283539354448,339.68939039302));
#28130=CARTESIAN_POINT('Ctrl Pts',(36.3865615724017,-1.35274364423431,339.730526795435));
#28131=CARTESIAN_POINT('Ctrl Pts',(36.3787864936232,-1.22073323610408,339.766310646383));
#28132=CARTESIAN_POINT('Ctrl Pts',(36.3710114148448,-1.08728409989692,339.796560887616));
#28133=CARTESIAN_POINT('Ctrl Pts',(36.3632459037958,-0.953999181347643,
339.826773904003));
#28134=CARTESIAN_POINT('Ctrl Pts',(36.3554803927467,-0.819279434961304,
339.851466773961));
#28135=CARTESIAN_POINT('Ctrl Pts',(36.3477148816977,-0.683621648717045,
339.870507622816));
#28136=CARTESIAN_POINT('Ctrl Pts',(36.3399570701755,-0.548098367562711,
339.889529592614));
#28137=CARTESIAN_POINT('Ctrl Pts',(36.3321992586534,-0.411639282027383,
339.902910639596));
#28138=CARTESIAN_POINT('Ctrl Pts',(36.3244414471312,-0.274752774587812,
339.910569618217));
#28139=CARTESIAN_POINT('Ctrl Pts',(36.3166894736082,-0.137969278586197,
339.918222833214));
#28140=CARTESIAN_POINT('Ctrl Pts',(36.3089375000852,-0.000759389598527255,
339.920162529059));
#28141=CARTESIAN_POINT('Ctrl Pts',(36.3011855265622,0.136362314299225,339.916359260849));
#28142=CARTESIAN_POINT('Ctrl Pts',(36.2934368360046,0.273425947074154,339.912557603326));
#28143=CARTESIAN_POINT('Ctrl Pts',(36.2856881454469,0.41040107912774,339.903017829935));
#28144=CARTESIAN_POINT('Ctrl Pts',(36.2779394548893,0.546772269625293,339.887762591173));
#28145=CARTESIAN_POINT('Ctrl Pts',(36.2701923765115,0.683115086957668,339.872510526391));
#28146=CARTESIAN_POINT('Ctrl Pts',(36.2624452981337,0.818853824463417,339.851545404969));
#28147=CARTESIAN_POINT('Ctrl Pts',(36.2546982197558,0.953477699854415,339.824941796372));
#28148=CARTESIAN_POINT('Ctrl Pts',(36.24695107645,1.08810270352297,339.798337964812));
#28149=CARTESIAN_POINT('Ctrl Pts',(36.2392039331442,1.22161244298154,339.766095627597));
#28150=CARTESIAN_POINT('Ctrl Pts',(36.2314567898384,1.35350626344092,339.728340497186));
#28151=CARTESIAN_POINT('Ctrl Pts',(36.2237079048104,1.48542973643115,339.690576878619));
#28152=CARTESIAN_POINT('Ctrl Pts',(36.2159590197822,1.61573619180197,339.647298108151));
#28153=CARTESIAN_POINT('Ctrl Pts',(36.2082101347542,1.74394045452447,339.598679675034));
#28154=CARTESIAN_POINT('Ctrl Pts',(36.2004530249794,1.8722807945762,339.550009637811));
#28155=CARTESIAN_POINT('Ctrl Pts',(36.1926959152047,1.99851411871656,339.495988755248));
#28156=CARTESIAN_POINT('Ctrl Pts',(36.18493880543,2.12217504601478,339.436840783325));
#28157=CARTESIAN_POINT('Ctrl Pts',(36.1771775505038,2.24590205375872,339.377661204616));
#28158=CARTESIAN_POINT('Ctrl Pts',(36.1694162955776,2.3670535805621,339.313349260521));
#28159=CARTESIAN_POINT('Ctrl Pts',(36.1616550406515,2.4851900520218,339.244174061915));
#28160=CARTESIAN_POINT('Ctrl Pts',(36.1538813702468,2.60351550333524,339.174888205535));
#28161=CARTESIAN_POINT('Ctrl Pts',(36.1461076998422,2.71881593239847,339.100723760221));
#28162=CARTESIAN_POINT('Ctrl Pts',(36.1383340294375,2.83068115600148,339.021992945737));
#28163=CARTESIAN_POINT('Ctrl Pts',(36.1309222252604,2.93733902653271,338.946927069609));
#28164=CARTESIAN_POINT('Ctrl Pts',(36.1235104210833,3.04087408336792,338.867710560901));
#28165=CARTESIAN_POINT('Ctrl Pts',(36.1160986169062,3.14096110872323,338.784646136165));
#28166=CARTESIAN_POINT('Ctrl Pts',(36.1083235381278,3.2459536973347,338.697510476537));
#28167=CARTESIAN_POINT('Ctrl Pts',(36.1005484593493,3.3474835076065,338.605864803047));
#28168=CARTESIAN_POINT('Ctrl Pts',(36.0927733805709,3.445138565732,338.510014718688));
#28169=CARTESIAN_POINT('Ctrl Pts',(36.0850078695219,3.54267345309158,338.41428258396));
#28170=CARTESIAN_POINT('Ctrl Pts',(36.0772423584729,3.63634279922566,338.314356603915));
#28171=CARTESIAN_POINT('Ctrl Pts',(36.0694768474239,3.72576686742553,338.210583173209));
#28172=CARTESIAN_POINT('Ctrl Pts',(36.0617190359017,3.81510227140124,338.106912634163));
#28173=CARTESIAN_POINT('Ctrl Pts',(36.0539612243796,3.90020052048451,337.999402530236));
#28174=CARTESIAN_POINT('Ctrl Pts',(36.0462034128574,3.98071826272555,337.888436458589));
#28175=CARTESIAN_POINT('Ctrl Pts',(36.0384514393344,4.06117541281218,337.777553892429));
#28176=CARTESIAN_POINT('Ctrl Pts',(36.0306994658114,4.13705868846306,337.663220850256));
#28177=CARTESIAN_POINT('Ctrl Pts',(36.0229474922884,4.20806486110713,337.545854117426));
#28178=CARTESIAN_POINT('Ctrl Pts',(36.0151988017308,4.27904096259503,337.428537089476));
#28179=CARTESIAN_POINT('Ctrl Pts',(36.0074501111731,4.34514386721381,337.308189259922));
#28180=CARTESIAN_POINT('Ctrl Pts',(35.9997014206155,4.40611368763817,337.185256331442));
#28181=CARTESIAN_POINT('Ctrl Pts',(35.9919543422377,4.46707082278208,337.062348980184));
#28182=CARTESIAN_POINT('Ctrl Pts',(35.9842072638599,4.5228968244588,336.936857949777));
#28183=CARTESIAN_POINT('Ctrl Pts',(35.9764601854821,4.573377986117,336.809253121761));
#28184=CARTESIAN_POINT('Ctrl Pts',(35.9687130421763,4.62385957085595,336.681647224292));
#28185=CARTESIAN_POINT('Ctrl Pts',(35.9609658988705,4.66899608244052,336.551927857345));
#28186=CARTESIAN_POINT('Ctrl Pts',(35.9532187555647,4.70862230212363,336.420584062435));
#28187=CARTESIAN_POINT('Ctrl Pts',(35.9454698705367,4.74825743062217,336.289210738651));
#28188=CARTESIAN_POINT('Ctrl Pts',(35.9377209855086,4.78237968920694,336.156212634328));
#28189=CARTESIAN_POINT('Ctrl Pts',(35.9299721004805,4.8108740944889,336.022092710802));
#28190=CARTESIAN_POINT('Ctrl Pts',(35.9222149907058,4.83939874402706,335.887830431004));
#28191=CARTESIAN_POINT('Ctrl Pts',(35.9144578809311,4.86228352635401,335.752444336393));
#28192=CARTESIAN_POINT('Ctrl Pts',(35.9067007711564,4.87946475832095,335.61644686292));
#28193=CARTESIAN_POINT('Ctrl Pts',(35.8989395162302,4.89665517138892,335.480376716746));
#28194=CARTESIAN_POINT('Ctrl Pts',(35.891178261304,4.90813592839074,335.343694930034));
#28195=CARTESIAN_POINT('Ctrl Pts',(35.8834170063779,4.91389545147088,335.206916781615));
#28196=CARTESIAN_POINT('Ctrl Pts',(35.8756433359732,4.91966418791092,335.069919832734));
#28197=CARTESIAN_POINT('Ctrl Pts',(35.8678696655686,4.91969340172038,334.932826605193));
#28198=CARTESIAN_POINT('Ctrl Pts',(35.8600959951639,4.91402367148986,334.796150990836));
#28199=CARTESIAN_POINT('Ctrl Pts',(35.8526841909867,4.90861786856551,334.665837659206));
#28200=CARTESIAN_POINT('Ctrl Pts',(35.8452723868095,4.8980317764762,334.535904222782));
#28201=CARTESIAN_POINT('Ctrl Pts',(35.8378605826322,4.88234396202589,334.406787981436));
#28202=CARTESIAN_POINT('Ctrl Pts',(35.8300855038538,4.8658872410581,334.271343368485));
#28203=CARTESIAN_POINT('Ctrl Pts',(35.8223104250754,4.84376404516267,334.136370052431));
#28204=CARTESIAN_POINT('Ctrl Pts',(35.8145353462969,4.81600841975109,334.00237985015));
#28205=CARTESIAN_POINT('Ctrl Pts',(35.8067698352479,4.78828694940359,333.868554531344));
#28206=CARTESIAN_POINT('Ctrl Pts',(35.7990043241989,4.75494691889533,333.735710298277));
#28207=CARTESIAN_POINT('Ctrl Pts',(35.7912388131498,4.71607412156075,333.604353933676));
#28208=CARTESIAN_POINT('Ctrl Pts',(35.7834810016276,4.67723986671793,333.473127809293));
#28209=CARTESIAN_POINT('Ctrl Pts',(35.7757231901055,4.63288387221369,333.343386989984));
#28210=CARTESIAN_POINT('Ctrl Pts',(35.7679653785833,4.58314290564166,333.215627794162));
#28211=CARTESIAN_POINT('Ctrl Pts',(35.7602134050602,4.53343937072436,333.087964741187));
#28212=CARTESIAN_POINT('Ctrl Pts',(35.7524614315372,4.47835907100887,332.962280706245));
#28213=CARTESIAN_POINT('Ctrl Pts',(35.7447094580142,4.41808839581309,332.839056227182));
#28214=CARTESIAN_POINT('Ctrl Pts',(35.7369607674566,4.35784324528403,332.715883933759));
#28215=CARTESIAN_POINT('Ctrl Pts',(35.729212076899,4.2924122625766,332.595169474892));
#28216=CARTESIAN_POINT('Ctrl Pts',(35.7214633863413,4.22202960863737,332.477372590673));
#28217=CARTESIAN_POINT('Ctrl Pts',(35.7137163079635,4.15166159839713,332.359600215079));
#28218=CARTESIAN_POINT('Ctrl Pts',(35.7059692295857,4.07634416649656,332.244744542046));
#28219=CARTESIAN_POINT('Ctrl Pts',(35.6982221512078,3.99635679746895,332.133239561836));
#28220=CARTESIAN_POINT('Ctrl Pts',(35.690475007902,3.91636875807015,332.021733647106));
#28221=CARTESIAN_POINT('Ctrl Pts',(35.6827278645962,3.83171093131317,331.913578798818));
#28222=CARTESIAN_POINT('Ctrl Pts',(35.6749807212904,3.74270515329863,331.809178601367));
#28223=CARTESIAN_POINT('Ctrl Pts',(35.6672318362623,3.65367936489567,331.704754932536));
#28224=CARTESIAN_POINT('Ctrl Pts',(35.6594829512342,3.56030393363461,331.604087891646));
#28225=CARTESIAN_POINT('Ctrl Pts',(35.6517340662061,3.46293958632525,331.507546351924));
#28226=CARTESIAN_POINT('Ctrl Pts',(35.6439769564314,3.36547189549168,331.410902342014));
#28227=CARTESIAN_POINT('Ctrl Pts',(35.6362198466566,3.26400710904246,331.318392856083));
#28228=CARTESIAN_POINT('Ctrl Pts',(35.6284627368819,3.15894168269649,331.230348755147));
#28229=CARTESIAN_POINT('Ctrl Pts',(35.6207014819557,3.05382011274594,331.142257606259));
#28230=CARTESIAN_POINT('Ctrl Pts',(35.6129402270296,2.94509437870116,331.058636835176));
#28231=CARTESIAN_POINT('Ctrl Pts',(35.6051789721034,2.83319152408137,330.979775024906));
#28232=CARTESIAN_POINT('Ctrl Pts',(35.5974053016987,2.72110966136323,330.90078706144));
#28233=CARTESIAN_POINT('Ctrl Pts',(35.5896316312941,2.60584085083701,330.826573483094));
#28234=CARTESIAN_POINT('Ctrl Pts',(35.5818579608894,2.48783919452025,330.75737826283));
#28235=CARTESIAN_POINT('Ctrl Pts',(35.5744461567124,2.37533054369523,330.691404096716));
#28236=CARTESIAN_POINT('Ctrl Pts',(35.5670343525354,2.2603380031423,330.629991729373));
#28237=CARTESIAN_POINT('Ctrl Pts',(35.5596225483583,2.14327182465691,330.573311740349));
#28238=CARTESIAN_POINT('Ctrl Pts',(35.5518474695799,2.02046788404084,330.513853696222));
#28239=CARTESIAN_POINT('Ctrl Pts',(35.5440723908014,1.89499381231326,330.459415757544));
#28240=CARTESIAN_POINT('Ctrl Pts',(35.536297312023,1.76729843113215,330.410246268282));
#28241=CARTESIAN_POINT('Ctrl Pts',(35.528531800974,1.63976018724706,330.361137285208));
#28242=CARTESIAN_POINT('Ctrl Pts',(35.5207662899249,1.5100064339957,330.317283991028));
#28243=CARTESIAN_POINT('Ctrl Pts',(35.5130007788759,1.37850976347893,330.278888489509));
#28244=CARTESIAN_POINT('Ctrl Pts',(35.5052429673537,1.24714347229373,330.240531057241));
#28245=CARTESIAN_POINT('Ctrl Pts',(35.4974851558314,1.11403807566469,330.207620757459));
#28246=CARTESIAN_POINT('Ctrl Pts',(35.4897273443092,0.979684951126885,330.180311165746));
#28247=CARTESIAN_POINT('Ctrl Pts',(35.4819753707862,0.845432931576058,330.153022125367));
#28248=CARTESIAN_POINT('Ctrl Pts',(35.4742233972632,0.709935434559029,330.131325481429));
#28249=CARTESIAN_POINT('Ctrl Pts',(35.4664714237402,0.573697420556687,330.115324541779));
#28250=CARTESIAN_POINT('Ctrl Pts',(35.4587227331826,0.437517103434159,330.099330378537));
#28251=CARTESIAN_POINT('Ctrl Pts',(35.450974042625,0.300597280471339,330.089027167518));
#28252=CARTESIAN_POINT('Ctrl Pts',(35.4432253520673,0.163451274842229,330.084466789528));
#28253=CARTESIAN_POINT('Ctrl Pts',(35.4354782736895,0.0263338035848693,
330.079907360363));
#28254=CARTESIAN_POINT('Ctrl Pts',(35.4277311953116,-0.111009366321611,
330.08108840058));
#28255=CARTESIAN_POINT('Ctrl Pts',(35.4199841169338,-0.248062038090289,
330.088009742705));
#28256=CARTESIAN_POINT('Ctrl Pts',(35.412236973628,-0.385115858491988,330.094931142838));
#28257=CARTESIAN_POINT('Ctrl Pts',(35.4044898303222,-0.521878785522984,
330.107592921121));
#28258=CARTESIAN_POINT('Ctrl Pts',(35.3967426870164,-0.657837272474206,
330.125942841385));
#28259=CARTESIAN_POINT('Ctrl Pts',(35.3889938019883,-0.793826325779775,
330.144296887102));
#28260=CARTESIAN_POINT('Ctrl Pts',(35.3812449169602,-0.92901019183751,330.168341567228));
#28261=CARTESIAN_POINT('Ctrl Pts',(35.3734960319321,-1.0628834673078,330.197973157361));
#28262=CARTESIAN_POINT('Ctrl Pts',(35.3657389221574,-1.19689883725602,330.227636198771));
#28263=CARTESIAN_POINT('Ctrl Pts',(35.3579818123826,-1.32960045557487,330.262897911322));
#28264=CARTESIAN_POINT('Ctrl Pts',(35.3502247026078,-1.46049554923932,330.303603954823));
#28265=CARTESIAN_POINT('Ctrl Pts',(35.3424634476817,-1.59146058905669,330.344331750333));
#28266=CARTESIAN_POINT('Ctrl Pts',(35.3347021927555,-1.72061681280448,330.390509542261));
#28267=CARTESIAN_POINT('Ctrl Pts',(35.3269409378293,-1.84749044712313,330.441934389427));
#28268=CARTESIAN_POINT('Ctrl Pts',(35.3191672674246,-1.97456703790849,330.493441499589));
#28269=CARTESIAN_POINT('Ctrl Pts',(35.31139359702,-2.09935338671523,330.550212275896));
#28270=CARTESIAN_POINT('Ctrl Pts',(35.3036199266153,-2.22139859081782,330.611996882042));
#28271=CARTESIAN_POINT('Ctrl Pts',(35.2962081224383,-2.33776256130557,330.670905399906));
#28272=CARTESIAN_POINT('Ctrl Pts',(35.2887963182613,-2.45163459314333,330.734371324704));
#28273=CARTESIAN_POINT('Ctrl Pts',(35.2813845140843,-2.56264923156155,330.802141977332));
#28274=CARTESIAN_POINT('Ctrl Pts',(35.2736094353059,-2.67910502810576,330.873234271524));
#28275=CARTESIAN_POINT('Ctrl Pts',(35.2658343565274,-2.79278427203539,330.949288603045));
#28276=CARTESIAN_POINT('Ctrl Pts',(35.258059277749,-2.90323524245689,331.030061941358));
#28277=CARTESIAN_POINT('Ctrl Pts',(35.2502937666999,-3.01355029592763,331.110735882935));
#28278=CARTESIAN_POINT('Ctrl Pts',(35.2425282556509,-3.12064466772559,331.196117048437));
#28279=CARTESIAN_POINT('Ctrl Pts',(35.2347627446019,-3.22409265777899,331.285917395028));
#28280=CARTESIAN_POINT('Ctrl Pts',(35.2270049330797,-3.327438078849,331.375628704314));
#28281=CARTESIAN_POINT('Ctrl Pts',(35.2192471215575,-3.42714401974859,331.469750220413));
#28282=CARTESIAN_POINT('Ctrl Pts',(35.2114893100353,-3.52281542291247,331.567951842035));
#28283=CARTESIAN_POINT('Ctrl Pts',(35.2037373365123,-3.61841483031169,331.666079563823));
#28284=CARTESIAN_POINT('Ctrl Pts',(35.1959853629892,-3.70998547155759,331.768281000789));
#28285=CARTESIAN_POINT('Ctrl Pts',(35.1882333894662,-3.79716720978638,331.874187426696));
#28286=CARTESIAN_POINT('Ctrl Pts',(35.1804846989086,-3.88431202649716,331.980049001169));
#28287=CARTESIAN_POINT('Ctrl Pts',(35.1727360083509,-3.96707138911558,332.089612142674));
#28288=CARTESIAN_POINT('Ctrl Pts',(35.1649873177933,-4.04512388134036,332.202473262485));
#28289=CARTESIAN_POINT('Ctrl Pts',(35.1572402394155,-4.12316013409223,332.315310900597));
#28290=CARTESIAN_POINT('Ctrl Pts',(35.1494931610376,-4.19649124216299,332.431444830889));
#28291=CARTESIAN_POINT('Ctrl Pts',(35.1417460826597,-4.2648380026844,332.55044088184));
#28292=CARTESIAN_POINT('Ctrl Pts',(35.1339989393539,-4.33318533601741,332.669437930093));
#28293=CARTESIAN_POINT('Ctrl Pts',(35.1262517960481,-4.39654804380354,332.791296807904));
#28294=CARTESIAN_POINT('Ctrl Pts',(35.1185046527423,-4.45469214296026,332.915557394902));
#28295=CARTESIAN_POINT('Ctrl Pts',(35.1107557677142,-4.5128493141449,333.039845918318));
#28296=CARTESIAN_POINT('Ctrl Pts',(35.1030068826861,-4.56578537642855,333.166536871407));
#28297=CARTESIAN_POINT('Ctrl Pts',(35.095257997658,-4.61331405112678,333.295149118493));
#28298=CARTESIAN_POINT('Ctrl Pts',(35.0875008878833,-4.6608931732514,333.423897875946));
#28299=CARTESIAN_POINT('Ctrl Pts',(35.0797437781085,-4.70305330698094,333.554571633834));
#28300=CARTESIAN_POINT('Ctrl Pts',(35.0719866683338,-4.73965757251598,333.686672486471));
#28301=CARTESIAN_POINT('Ctrl Pts',(35.0642254134076,-4.77628139820017,333.818843929581));
#28302=CARTESIAN_POINT('Ctrl Pts',(35.0564641584814,-4.80734335145991,333.952443606451));
#28303=CARTESIAN_POINT('Ctrl Pts',(35.0487029035552,-4.8327577039145,334.086963287838));
#28304=CARTESIAN_POINT('Ctrl Pts',(35.0409292331506,-4.8582127110505,334.221698156876));
#28305=CARTESIAN_POINT('Ctrl Pts',(35.0331555627459,-4.87800200768101,334.357355584354));
#28306=CARTESIAN_POINT('Ctrl Pts',(35.0253818923412,-4.89209167714841,334.49342119579));
#28307=CARTESIAN_POINT('Ctrl Pts',(35.0179700881642,-4.90552546911202,334.623152920274));
#28308=CARTESIAN_POINT('Ctrl Pts',(35.0105582839873,-4.91377830936601,334.753255394781));
#28309=CARTESIAN_POINT('Ctrl Pts',(35.0031464798104,-4.91686491261461,334.883284561436));
#28310=CARTESIAN_POINT('Ctrl Pts',(35.0009430693703,-4.91778251022781,334.921940146024));
#28311=CARTESIAN_POINT('Ctrl Pts',(34.9987396589303,-4.91824426091572,334.960606594331));
#28312=CARTESIAN_POINT('Ctrl Pts',(34.9965362484902,-4.91824994683472,334.999276840106));
#28313=CARTESIAN_POINT('',(38.4965362485229,-4.91824977738391,334.998520215163));
#28314=CARTESIAN_POINT('Ctrl Pts',(38.4965362484901,-4.91824977738408,334.998520215746));
#28315=CARTESIAN_POINT('Ctrl Pts',(38.4885838555402,-4.91829224990027,335.139682985052));
#28316=CARTESIAN_POINT('Ctrl Pts',(38.4806314625904,-4.91225292694631,335.280790264135));
#28317=CARTESIAN_POINT('Ctrl Pts',(38.4726790696405,-4.90017238107107,335.421300009837));
#28318=CARTESIAN_POINT('Ctrl Pts',(38.4647215384514,-4.88808402965417,335.561900542385));
#28319=CARTESIAN_POINT('Ctrl Pts',(38.4567640072624,-4.86994670554018,335.701902412536));
#28320=CARTESIAN_POINT('Ctrl Pts',(38.4488064760733,-4.84585267460449,335.840770431526));
#28321=CARTESIAN_POINT('Ctrl Pts',(38.4408425052537,-4.82173914557912,335.979750829433));
#28322=CARTESIAN_POINT('Ctrl Pts',(38.4328785344342,-4.79165936241612,336.117595192121));
#28323=CARTESIAN_POINT('Ctrl Pts',(38.4249145636146,-4.75575631911382,336.253780242191));
#28324=CARTESIAN_POINT('Ctrl Pts',(38.4169371080535,-4.71979248411985,336.390195883287));
#28325=CARTESIAN_POINT('Ctrl Pts',(38.4089596524924,-4.67798578106659,336.524946249112));
#28326=CARTESIAN_POINT('Ctrl Pts',(38.4009821969313,-4.63052889546794,336.657523819056));
#28327=CARTESIAN_POINT('Ctrl Pts',(38.3929971971094,-4.58302713000514,336.790226767292));
#28328=CARTESIAN_POINT('Ctrl Pts',(38.3850121972875,-4.52986466195102,336.920752488628));
#28329=CARTESIAN_POINT('Ctrl Pts',(38.3770271974656,-4.47128147023148,337.048615404722));
#28330=CARTESIAN_POINT('Ctrl Pts',(38.3690276478814,-4.4125915319209,337.176711304544));
#28331=CARTESIAN_POINT('Ctrl Pts',(38.3610280982973,-4.34846129757621,337.302134383415));
#28332=CARTESIAN_POINT('Ctrl Pts',(38.3530285487132,-4.27917616809477,337.424424547168));
#28333=CARTESIAN_POINT('Ctrl Pts',(38.349353329508,-4.24734462110284,337.480608105217));
#28334=CARTESIAN_POINT('Ctrl Pts',(38.3456781103028,-4.21442560091628,337.536130803463));
#28335=CARTESIAN_POINT('Ctrl Pts',(38.3420028910976,-4.18044970707607,337.590950271446));
#28336=CARTESIAN_POINT('Ctrl Pts',(38.3342278123192,-4.10857229339569,337.706923131395));
#28337=CARTESIAN_POINT('Ctrl Pts',(38.3264527335408,-4.03175171321087,337.820085979996));
#28338=CARTESIAN_POINT('Ctrl Pts',(38.3186776547624,-3.95023404320812,337.929988748507));
#28339=CARTESIAN_POINT('Ctrl Pts',(38.3109121437134,-3.86881668588808,338.039756274665));
#28340=CARTESIAN_POINT('Ctrl Pts',(38.3031466326644,-3.78271397006088,338.146271391997));
#28341=CARTESIAN_POINT('Ctrl Pts',(38.2953811216154,-3.69221680789574,338.249110356081));
#28342=CARTESIAN_POINT('Ctrl Pts',(38.2876233100932,-3.60180937393031,338.351847355032));
#28343=CARTESIAN_POINT('Ctrl Pts',(38.279865498571,-3.50701642107217,338.45091516278));
#28344=CARTESIAN_POINT('Ctrl Pts',(38.2721076870488,-3.40817071197461,338.545920960842));
#28345=CARTESIAN_POINT('Ctrl Pts',(38.2643557135258,-3.30939938740772,338.640855264028));
#28346=CARTESIAN_POINT('Ctrl Pts',(38.2566037400028,-3.20658165780887,338.731733372152));
#28347=CARTESIAN_POINT('Ctrl Pts',(38.2488517664798,-3.10008867398177,338.818197647575));
#28348=CARTESIAN_POINT('Ctrl Pts',(38.2411030759222,-2.99364078999656,338.904625305327));
#28349=CARTESIAN_POINT('Ctrl Pts',(38.2333543853646,-2.88352105031383,338.986642602341));
#28350=CARTESIAN_POINT('Ctrl Pts',(38.225605694807,-2.7701352058464,339.063930856182));
#28351=CARTESIAN_POINT('Ctrl Pts',(38.2178586164292,-2.65677295225092,339.141203029556));
#28352=CARTESIAN_POINT('Ctrl Pts',(38.2101115380514,-2.54014626829974,339.21374789682));
#28353=CARTESIAN_POINT('Ctrl Pts',(38.2023644596735,-2.42069120181971,339.281289194616));
#28354=CARTESIAN_POINT('Ctrl Pts',(38.1946173163677,-2.30123513419133,339.348831058472));
#28355=CARTESIAN_POINT('Ctrl Pts',(38.1868701730619,-2.17895097700587,339.411369076835));
#28356=CARTESIAN_POINT('Ctrl Pts',(38.1791230297561,-2.0543004208578,339.468672380402));
#28357=CARTESIAN_POINT('Ctrl Pts',(38.1713741447281,-1.9296218406183,339.525988566968));
#28358=CARTESIAN_POINT('Ctrl Pts',(38.1636252597,-1.80257615783736,339.578067533656));
#28359=CARTESIAN_POINT('Ctrl Pts',(38.1558763746719,-1.67364575565692,339.624726256447));
#28360=CARTESIAN_POINT('Ctrl Pts',(38.1481192648972,-1.54457850541533,339.671434503289));
#28361=CARTESIAN_POINT('Ctrl Pts',(38.1403621551225,-1.41362290779365,339.712710880649));
#28362=CARTESIAN_POINT('Ctrl Pts',(38.1326050453478,-1.28127778183339,339.748421875558));
#28363=CARTESIAN_POINT('Ctrl Pts',(38.1248437904216,-1.14886193486967,339.784151953282));
#28364=CARTESIAN_POINT('Ctrl Pts',(38.1170825354954,-1.0150554611458,339.814310636767));
#28365=CARTESIAN_POINT('Ctrl Pts',(38.1093212805692,-0.880367157463933,
339.838815633041));
#28366=CARTESIAN_POINT('Ctrl Pts',(38.1015476101646,-0.745463396390805,
339.863359829322));
#28367=CARTESIAN_POINT('Ctrl Pts',(38.09377393976,-0.609675373838679,339.882232211851));
#28368=CARTESIAN_POINT('Ctrl Pts',(38.0860002693553,-0.473517681683084,
339.89540233971));
#28369=CARTESIAN_POINT('Ctrl Pts',(38.0785884651781,-0.343698162852952,
339.907959394948));
#28370=CARTESIAN_POINT('Ctrl Pts',(38.0711766610009,-0.213542903478925,
339.915333112026));
#28371=CARTESIAN_POINT('Ctrl Pts',(38.0637648568238,-0.083495851893928,
339.917541205238));
#28372=CARTESIAN_POINT('Ctrl Pts',(38.0559897780453,0.0529251930775802,
339.919857523677));
#28373=CARTESIAN_POINT('Ctrl Pts',(38.0482146992669,0.189658270591596,339.916496369565));
#28374=CARTESIAN_POINT('Ctrl Pts',(38.0404396204885,0.326191742027135,339.907421116017));
#28375=CARTESIAN_POINT('Ctrl Pts',(38.0326741094394,0.462557200333927,339.898357030147));
#28376=CARTESIAN_POINT('Ctrl Pts',(38.0249085983904,0.598723155006201,339.883592861312));
#28377=CARTESIAN_POINT('Ctrl Pts',(38.0171430873414,0.734175841051302,339.863143931339));
#28378=CARTESIAN_POINT('Ctrl Pts',(38.0093852758192,0.86949422536337,339.84271527654));
#28379=CARTESIAN_POINT('Ctrl Pts',(38.001627464297,1.00410036442694,339.816613135444));
#28380=CARTESIAN_POINT('Ctrl Pts',(37.9938696527748,1.13748385183549,339.784904758646));
#28381=CARTESIAN_POINT('Ctrl Pts',(37.9861176792518,1.27076696394048,339.753220243407));
#28382=CARTESIAN_POINT('Ctrl Pts',(37.9783657057288,1.40282887702735,339.715937979958));
#28383=CARTESIAN_POINT('Ctrl Pts',(37.9706137322058,1.53316799498063,339.67317653868));
#28384=CARTESIAN_POINT('Ctrl Pts',(37.9628650416482,1.6634519142399,339.630433206898));
#28385=CARTESIAN_POINT('Ctrl Pts',(37.9551163510905,1.79201411887373,339.582215434063));
#28386=CARTESIAN_POINT('Ctrl Pts',(37.9473676605329,1.91836704692088,339.528691967421));
#28387=CARTESIAN_POINT('Ctrl Pts',(37.9396205821551,2.04469368618603,339.475179636784));
#28388=CARTESIAN_POINT('Ctrl Pts',(37.9318735037772,2.16881160346916,339.416363960429));
#28389=CARTESIAN_POINT('Ctrl Pts',(37.9241264253994,2.29025251251831,339.352462118319));
#28390=CARTESIAN_POINT('Ctrl Pts',(37.9163792820936,2.41169443935891,339.288559740651));
#28391=CARTESIAN_POINT('Ctrl Pts',(37.9086321387878,2.53045896730672,339.219571294222));
#28392=CARTESIAN_POINT('Ctrl Pts',(37.900884995482,2.64610210616758,339.145760087877));
#28393=CARTESIAN_POINT('Ctrl Pts',(37.8931361104539,2.76177124406138,339.071932287206));
#28394=CARTESIAN_POINT('Ctrl Pts',(37.8853872254259,2.87431726703825,338.99327977932));
#28395=CARTESIAN_POINT('Ctrl Pts',(37.8776383403978,2.98332522109835,338.910109165696));
#28396=CARTESIAN_POINT('Ctrl Pts',(37.869881230623,3.09244887732715,338.826850273923));
#28397=CARTESIAN_POINT('Ctrl Pts',(37.8621241208483,3.19802665174555,338.739063934295));
#28398=CARTESIAN_POINT('Ctrl Pts',(37.8543670110736,3.29967633084447,338.647097362858));
#28399=CARTESIAN_POINT('Ctrl Pts',(37.8466057561474,3.4013803282817,338.555081647425));
#28400=CARTESIAN_POINT('Ctrl Pts',(37.8388445012213,3.4991517693778,338.458881523174));
#28401=CARTESIAN_POINT('Ctrl Pts',(37.8310832462951,3.59264611307092,338.358880314738));
#28402=CARTESIAN_POINT('Ctrl Pts',(37.8233095758905,3.68629001724434,338.25871913696));
#28403=CARTESIAN_POINT('Ctrl Pts',(37.8155359054858,3.77564289685556,338.154745020968));
#28404=CARTESIAN_POINT('Ctrl Pts',(37.8077622350811,3.86040067829626,338.047374224724));
#28405=CARTESIAN_POINT('Ctrl Pts',(37.800350430904,3.94121296461935,337.945001564876));
#28406=CARTESIAN_POINT('Ctrl Pts',(37.7929386267269,4.01784815977472,337.839541571944));
#28407=CARTESIAN_POINT('Ctrl Pts',(37.7855268225499,4.09008091417473,337.731377157773));
#28408=CARTESIAN_POINT('Ctrl Pts',(37.7777517437714,4.16585401103821,337.617911283458));
#28409=CARTESIAN_POINT('Ctrl Pts',(37.769976664993,4.2370216588236,337.501110608152));
#28410=CARTESIAN_POINT('Ctrl Pts',(37.7622015862146,4.30327618018612,337.381385558775));
#28411=CARTESIAN_POINT('Ctrl Pts',(37.7544360751655,4.36944917114231,337.261807838694));
#28412=CARTESIAN_POINT('Ctrl Pts',(37.7466705641164,4.43072087786297,337.139313243511));
#28413=CARTESIAN_POINT('Ctrl Pts',(37.7389050530674,4.48682615708263,337.014342100692));
#28414=CARTESIAN_POINT('Ctrl Pts',(37.7311472415452,4.54287580775426,336.889494867125));
#28415=CARTESIAN_POINT('Ctrl Pts',(37.7233894300231,4.59376906598802,336.762176326803));
#28416=CARTESIAN_POINT('Ctrl Pts',(37.7156316185009,4.63928627404983,336.632852084517));
#28417=CARTESIAN_POINT('Ctrl Pts',(37.7078796449779,4.68476922896933,336.503625162825));
#28418=CARTESIAN_POINT('Ctrl Pts',(37.7001276714549,4.72488405713468,336.372395910684));
#28419=CARTESIAN_POINT('Ctrl Pts',(37.6923756979318,4.75945902447026,336.239650296208));
#28420=CARTESIAN_POINT('Ctrl Pts',(37.6846270073742,4.79401934928656,336.106960899578));
#28421=CARTESIAN_POINT('Ctrl Pts',(37.6768783168166,4.82304438125378,335.972756795332));
#28422=CARTESIAN_POINT('Ctrl Pts',(37.669129626259,4.84641217577767,335.83753930354));
#28423=CARTESIAN_POINT('Ctrl Pts',(37.6613825478812,4.86977510843673,335.702349944877));
#28424=CARTESIAN_POINT('Ctrl Pts',(37.6536354695033,4.88748307833829,335.566148002975));
#28425=CARTESIAN_POINT('Ctrl Pts',(37.6458883911255,4.89946530018679,335.429444798275));
#28426=CARTESIAN_POINT('Ctrl Pts',(37.6381412478197,4.91144762245785,335.292740447871));
#28427=CARTESIAN_POINT('Ctrl Pts',(37.6303941045139,4.9177040668318,335.155535215671));
#28428=CARTESIAN_POINT('Ctrl Pts',(37.6226469612081,4.9182157867627,335.018344954025));
#28429=CARTESIAN_POINT('Ctrl Pts',(37.61489807618,4.9187276217391,334.881123849096));
#28430=CARTESIAN_POINT('Ctrl Pts',(37.6071491911519,4.91349216080239,334.743918112213));
#28431=CARTESIAN_POINT('Ctrl Pts',(37.5994003061238,4.90254267625575,334.607242606701));
#28432=CARTESIAN_POINT('Ctrl Pts',(37.591643196349,4.89158156981306,334.470422032394));
#28433=CARTESIAN_POINT('Ctrl Pts',(37.5838860865743,4.87489435576975,334.334133203931));
#28434=CARTESIAN_POINT('Ctrl Pts',(37.5761289767996,4.85256617784498,334.19888543133));
#28435=CARTESIAN_POINT('Ctrl Pts',(37.5683677218734,4.83022606845586,334.063565386644));
#28436=CARTESIAN_POINT('Ctrl Pts',(37.5606064669472,4.80223906853414,333.92928788877));
#28437=CARTESIAN_POINT('Ctrl Pts',(37.5528452120211,4.76874107300531,333.796550108591));
#28438=CARTESIAN_POINT('Ctrl Pts',(37.5450715416164,4.73518949160061,333.663599991223));
#28439=CARTESIAN_POINT('Ctrl Pts',(37.5372978712118,4.69610940949782,333.532194888302));
#28440=CARTESIAN_POINT('Ctrl Pts',(37.5295242008071,4.65168631521807,333.402815762877));
#28441=CARTESIAN_POINT('Ctrl Pts',(37.52211239663,4.60933112666469,333.279459266868));
#28442=CARTESIAN_POINT('Ctrl Pts',(37.5147005924529,4.56211927014286,333.157944642853));
#28443=CARTESIAN_POINT('Ctrl Pts',(37.5072887882759,4.51025079480062,333.03866860768));
#28444=CARTESIAN_POINT('Ctrl Pts',(37.4995137094974,4.45584009097361,332.913546498717));
#28445=CARTESIAN_POINT('Ctrl Pts',(37.491738630719,4.39613280909055,332.79049255797));
#28446=CARTESIAN_POINT('Ctrl Pts',(37.4839635519405,4.33130758404089,332.669987623438));
#28447=CARTESIAN_POINT('Ctrl Pts',(37.4761980408915,4.26656213055763,332.549630977901));
#28448=CARTESIAN_POINT('Ctrl Pts',(37.4684325298425,4.19671144843798,332.431817438354));
#28449=CARTESIAN_POINT('Ctrl Pts',(37.4606670187935,4.12198233420488,332.317008255882));
#28450=CARTESIAN_POINT('Ctrl Pts',(37.4529092072713,4.04732731410615,332.20231290705));
#28451=CARTESIAN_POINT('Ctrl Pts',(37.4451513957492,3.96780369961219,332.090616312736));
#28452=CARTESIAN_POINT('Ctrl Pts',(37.437393584227,3.88368415832176,331.982355153286));
#28453=CARTESIAN_POINT('Ctrl Pts',(37.429641610704,3.79962791965396,331.874175463791));
#28454=CARTESIAN_POINT('Ctrl Pts',(37.421889637181,3.7109828771849,331.769426370709));
#28455=CARTESIAN_POINT('Ctrl Pts',(37.414137663658,3.61806475670521,331.668515274118));
#28456=CARTESIAN_POINT('Ctrl Pts',(37.4063889731004,3.52518598710445,331.567646913435));
#28457=CARTESIAN_POINT('Ctrl Pts',(37.3986402825428,3.42803800297779,331.470613603394));
#28458=CARTESIAN_POINT('Ctrl Pts',(37.3908915919852,3.32697638385219,331.377789182862));
#28459=CARTESIAN_POINT('Ctrl Pts',(37.3831445136074,3.2259357914404,331.284984075226));
#28460=CARTESIAN_POINT('Ctrl Pts',(37.3753974352296,3.12098347135104,331.196386379524));
#28461=CARTESIAN_POINT('Ctrl Pts',(37.3676503568517,3.01251109786592,331.112332325451));
#28462=CARTESIAN_POINT('Ctrl Pts',(37.359903213546,2.90403781527843,331.028277566924));
#28463=CARTESIAN_POINT('Ctrl Pts',(37.3521560702402,2.79204472942191,330.948766765397));
#28464=CARTESIAN_POINT('Ctrl Pts',(37.3444089269344,2.67695543259566,330.874094926638));
#28465=CARTESIAN_POINT('Ctrl Pts',(37.3366600419063,2.56184026125144,330.799406300064));
#28466=CARTESIAN_POINT('Ctrl Pts',(37.3289111568782,2.44362782162743,330.729559013768));
#28467=CARTESIAN_POINT('Ctrl Pts',(37.3211622718501,2.32276907882828,330.664803710449));
#28468=CARTESIAN_POINT('Ctrl Pts',(37.3134051620754,2.20178205531099,330.599979675181));
#28469=CARTESIAN_POINT('Ctrl Pts',(37.3056480523006,2.07814346283076,330.540258604143));
#28470=CARTESIAN_POINT('Ctrl Pts',(37.2978909425259,1.95232766720063,330.485844515041));
#28471=CARTESIAN_POINT('Ctrl Pts',(37.2901296875998,1.82644463963205,330.43140134879));
#28472=CARTESIAN_POINT('Ctrl Pts',(37.2823684326736,1.6983824554332,330.382270955159));
#28473=CARTESIAN_POINT('Ctrl Pts',(37.2746071777474,1.56863273674961,330.338608104901));
#28474=CARTESIAN_POINT('Ctrl Pts',(37.2668335073428,1.43867546080163,330.294875408312));
#28475=CARTESIAN_POINT('Ctrl Pts',(37.2590598369382,1.3070256315098,330.256627841875));
#28476=CARTESIAN_POINT('Ctrl Pts',(37.2512861665335,1.17418807944664,330.22396970104));
#28477=CARTESIAN_POINT('Ctrl Pts',(37.2438743623564,1.04753414738945,330.192831804517));
#28478=CARTESIAN_POINT('Ctrl Pts',(37.2364625581792,0.919800863073379,330.166774726325));
#28479=CARTESIAN_POINT('Ctrl Pts',(37.229050754002,0.791430092231746,330.145844927116));
#28480=CARTESIAN_POINT('Ctrl Pts',(37.2212756752235,0.656767487515261,330.1238892961));
#28481=CARTESIAN_POINT('Ctrl Pts',(37.2135005964451,0.520977767269429,330.107506875063));
#28482=CARTESIAN_POINT('Ctrl Pts',(37.2057255176667,0.384561948016524,330.096807655146));
#28483=CARTESIAN_POINT('Ctrl Pts',(37.1979600066176,0.248313997113864,330.0861216013));
#28484=CARTESIAN_POINT('Ctrl Pts',(37.1901944955686,0.111441866140478,330.081104863705));
#28485=CARTESIAN_POINT('Ctrl Pts',(37.1824289845195,-0.0255438364138864,
330.081816333755));
#28486=CARTESIAN_POINT('Ctrl Pts',(37.1746711729973,-0.162393717245253,
330.08252709838));
#28487=CARTESIAN_POINT('Ctrl Pts',(37.1669133614751,-0.299356557213057,
330.088954766037));
#28488=CARTESIAN_POINT('Ctrl Pts',(37.1591555499529,-0.43591758641646,330.101106357518));
#28489=CARTESIAN_POINT('Ctrl Pts',(37.1514035764298,-0.572375849115903,
330.11324880454));
#28490=CARTESIAN_POINT('Ctrl Pts',(37.1436516029067,-0.708432515145981,
330.131106567143));
#28491=CARTESIAN_POINT('Ctrl Pts',(37.1358996293836,-0.843574135747758,
330.154634612333));
#28492=CARTESIAN_POINT('Ctrl Pts',(37.128150938826,-0.978658523791689,330.178152693382));
#28493=CARTESIAN_POINT('Ctrl Pts',(37.1204022482683,-1.11282825288142,330.207336213962));
#28494=CARTESIAN_POINT('Ctrl Pts',(37.1126535577107,-1.24557652945232,330.242088465327));
#28495=CARTESIAN_POINT('Ctrl Pts',(37.1049064793328,-1.37829718663572,330.276833486195));
#28496=CARTESIAN_POINT('Ctrl Pts',(37.097159400955,-1.50959660166403,330.317144834339));
#28497=CARTESIAN_POINT('Ctrl Pts',(37.0894123225771,-1.63898007438538,330.36287509568));
#28498=CARTESIAN_POINT('Ctrl Pts',(37.0816651792713,-1.76836463146502,330.408605740284));
#28499=CARTESIAN_POINT('Ctrl Pts',(37.0739180359655,-1.89583284567782,330.459755258414));
#28500=CARTESIAN_POINT('Ctrl Pts',(37.0661708926596,-2.02090741028011,330.516127086817));
#28501=CARTESIAN_POINT('Ctrl Pts',(37.0584220076315,-2.14601009429959,330.572511588804));
#28502=CARTESIAN_POINT('Ctrl Pts',(37.0506731226034,-2.26871770158075,330.634120576785));
#28503=CARTESIAN_POINT('Ctrl Pts',(37.0429242375753,-2.38857541823775,330.700710461729));
#28504=CARTESIAN_POINT('Ctrl Pts',(37.0351671278005,-2.5085603531134,330.767371025864));
#28505=CARTESIAN_POINT('Ctrl Pts',(37.0274100180258,-2.62568901261414,330.839022857662));
#28506=CARTESIAN_POINT('Ctrl Pts',(37.0196529082511,-2.73953312733801,330.915377458477));
#28507=CARTESIAN_POINT('Ctrl Pts',(37.0118916533249,-2.85343807671698,330.99177286075));
#28508=CARTESIAN_POINT('Ctrl Pts',(37.0041303983987,-2.96405466894857,331.072875808435));
#28509=CARTESIAN_POINT('Ctrl Pts',(36.9963691434725,-3.07098670905383,331.158356641317));
#28510=CARTESIAN_POINT('Ctrl Pts',(36.9885954730679,-3.17808980557404,331.243974215673));
#28511=CARTESIAN_POINT('Ctrl Pts',(36.9808218026632,-3.28149627686227,331.333983412907));
#28512=CARTESIAN_POINT('Ctrl Pts',(36.9730481322585,-3.3808452258597,331.428016150473));
#28513=CARTESIAN_POINT('Ctrl Pts',(36.9656363280817,-3.4755694573765,331.51767164148));
#28514=CARTESIAN_POINT('Ctrl Pts',(36.9582245239048,-3.56660521980601,331.610984305163));
#28515=CARTESIAN_POINT('Ctrl Pts',(36.9508127197279,-3.65367432449124,331.707607709726));
#28516=CARTESIAN_POINT('Ctrl Pts',(36.9431146196332,-3.74410664933728,331.807963388596));
#28517=CARTESIAN_POINT('Ctrl Pts',(36.9354165195386,-3.83055911254457,331.912223196463));
#28518=CARTESIAN_POINT('Ctrl Pts',(36.9277184194439,-3.91267054438507,332.020034853626));
#28519=CARTESIAN_POINT('Ctrl Pts',(36.9200324550669,-3.99465253115025,332.127676550435));
#28520=CARTESIAN_POINT('Ctrl Pts',(36.9123464906898,-4.07230687213663,332.238858633726));
#28521=CARTESIAN_POINT('Ctrl Pts',(36.9046605263127,-4.14531014326032,332.353193078692));
#28522=CARTESIAN_POINT('Ctrl Pts',(36.8969815399504,-4.21824713540066,332.467423720491));
#28523=CARTESIAN_POINT('Ctrl Pts',(36.8893025535881,-4.28654124039229,332.584800699224));
#28524=CARTESIAN_POINT('Ctrl Pts',(36.8816235672258,-4.34991004158561,332.704903990546));
#28525=CARTESIAN_POINT('Ctrl Pts',(36.8739498084355,-4.41323570362541,332.824925519956));
#28526=CARTESIAN_POINT('Ctrl Pts',(36.8662760496453,-4.47164254473121,332.947669319001));
#28527=CARTESIAN_POINT('Ctrl Pts',(36.858602290855,-4.52489241493673,333.072687960981));
#28528=CARTESIAN_POINT('Ctrl Pts',(36.8509320135999,-4.57811812601729,333.197649882804));
#28529=CARTESIAN_POINT('Ctrl Pts',(36.8432617363449,-4.62619136494713,333.324884227468));
#28530=CARTESIAN_POINT('Ctrl Pts',(36.8355914590898,-4.66892097751543,333.453921098968));
#28531=CARTESIAN_POINT('Ctrl Pts',(36.8279210331352,-4.71165141845951,333.582960472036));
#28532=CARTESIAN_POINT('Ctrl Pts',(36.8202506071806,-4.74903788801809,333.713802066858));
#28533=CARTESIAN_POINT('Ctrl Pts',(36.812580181226,-4.7809382931974,333.845958363343));
#28534=CARTESIAN_POINT('Ctrl Pts',(36.8049099796634,-4.8128377651567,333.978110793704));
#28535=CARTESIAN_POINT('Ctrl Pts',(36.7972397781009,-4.83925140398853,334.11157745941));
#28536=CARTESIAN_POINT('Ctrl Pts',(36.7895695765383,-4.8600879060864,334.245859026698));
#28537=CARTESIAN_POINT('Ctrl Pts',(36.7818942818184,-4.88093824401132,334.380229759458));
#28538=CARTESIAN_POINT('Ctrl Pts',(36.7742189870985,-4.89620398947651,334.51541607898));
#28539=CARTESIAN_POINT('Ctrl Pts',(36.7665436923787,-4.90584553525493,334.65091169209));
#28540=CARTESIAN_POINT('Ctrl Pts',(36.7598745444158,-4.91422318037912,334.768645319935));
#28541=CARTESIAN_POINT('Ctrl Pts',(36.753205396453,-4.9183553271965,334.886612216886));
#28542=CARTESIAN_POINT('Ctrl Pts',(36.7465362484902,-4.91824795950011,335.004480108586));
#28543=CARTESIAN_POINT('',(40.2465362484602,-4.9182484758457,334.996128005489));
#28544=CARTESIAN_POINT('Ctrl Pts',(40.2465362484602,-4.91824847584569,334.996128005489));
#28545=CARTESIAN_POINT('Ctrl Pts',(40.2388859593559,-4.91835450293067,335.130804732851));
#28546=CARTESIAN_POINT('Ctrl Pts',(40.2312356702516,-4.91292458102749,335.265686434657));
#28547=CARTESIAN_POINT('Ctrl Pts',(40.2235853811473,-4.9019348286901,335.400272404463));
#28548=CARTESIAN_POINT('Ctrl Pts',(40.2159425957197,-4.89095585549429,335.534726367544));
#28549=CARTESIAN_POINT('Ctrl Pts',(40.2082998102923,-4.8744279304713,335.668884776161));
#28550=CARTESIAN_POINT('Ctrl Pts',(40.2006570248647,-4.85237921080569,335.802246257106));
#28551=CARTESIAN_POINT('Ctrl Pts',(40.1927726111929,-4.82963341630109,335.939823988893));
#28552=CARTESIAN_POINT('Ctrl Pts',(40.1848881975211,-4.80101195311241,336.076553133484));
#28553=CARTESIAN_POINT('Ctrl Pts',(40.1770037838493,-4.76660375329278,336.21188766872));
#28554=CARTESIAN_POINT('Ctrl Pts',(40.1693694278661,-4.73328682484401,336.342930008939));
#28555=CARTESIAN_POINT('Ctrl Pts',(40.1617350718829,-4.69454475515893,336.472664437365));
#28556=CARTESIAN_POINT('Ctrl Pts',(40.1541007158997,-4.65051021783986,336.600605440534));
#28557=CARTESIAN_POINT('Ctrl Pts',(40.146467469993,-4.60648208338,336.728527840391));
#28558=CARTESIAN_POINT('Ctrl Pts',(40.1388342240864,-4.55716314256936,336.854656952013));
#28559=CARTESIAN_POINT('Ctrl Pts',(40.1312009781797,-4.50273562993134,336.978523416451));
#28560=CARTESIAN_POINT('Ctrl Pts',(40.1235670762017,-4.44830343929241,337.102400527112));
#28561=CARTESIAN_POINT('Ctrl Pts',(40.1159331742237,-4.38876196647831,337.224014234624));
#28562=CARTESIAN_POINT('Ctrl Pts',(40.1082992722457,-4.32434094842294,337.342916649028));
#28563=CARTESIAN_POINT('Ctrl Pts',(40.1006629477018,-4.25989948680445,337.461856796288));
#28564=CARTESIAN_POINT('Ctrl Pts',(40.093026623158,-4.19057559340086,337.578083585273));
#28565=CARTESIAN_POINT('Ctrl Pts',(40.0853902986142,-4.11664386547576,337.69117564409));
#28566=CARTESIAN_POINT('Ctrl Pts',(40.077745772101,-4.04263272948421,337.804389172023));
#28567=CARTESIAN_POINT('Ctrl Pts',(40.0701012455878,-3.96400410309239,337.914460912896));
#28568=CARTESIAN_POINT('Ctrl Pts',(40.0624567190746,-3.88107476123571,338.021000125819));
#28569=CARTESIAN_POINT('Ctrl Pts',(40.0548072650216,-3.79809196444868,338.127608012219));
#28570=CARTESIAN_POINT('Ctrl Pts',(40.0471578109686,-3.71080319463436,338.230678532065));
#28571=CARTESIAN_POINT('Ctrl Pts',(40.0395083569156,-3.61956312757054,338.329856727854));
#28572=CARTESIAN_POINT('Ctrl Pts',(40.0318483389941,-3.5281970583026,338.429171888373));
#28573=CARTESIAN_POINT('Ctrl Pts',(40.0241883210727,-3.43286908885909,338.524583717112));
#28574=CARTESIAN_POINT('Ctrl Pts',(40.0165283031512,-3.33396819129148,338.615776425881));
#28575=CARTESIAN_POINT('Ctrl Pts',(40.0148292343479,-3.31203098025658,338.636003883329));
#28576=CARTESIAN_POINT('Ctrl Pts',(40.0131301655446,-3.28991809917468,338.656023927734));
#28577=CARTESIAN_POINT('Ctrl Pts',(40.0114310967413,-3.26763398618968,338.675833401393));
#28578=CARTESIAN_POINT('Ctrl Pts',(40.0036560179629,-3.16566004986063,338.766483184359));
#28579=CARTESIAN_POINT('Ctrl Pts',(39.9958809391844,-3.05974994568657,338.853029597787));
#28580=CARTESIAN_POINT('Ctrl Pts',(39.988105860406,-2.95026791490481,338.935111471456));
#28581=CARTESIAN_POINT('Ctrl Pts',(39.980340349357,-2.84092060873189,339.017092338154));
#28582=CARTESIAN_POINT('Ctrl Pts',(39.972574838308,-2.7280104314527,339.094619364151));
#28583=CARTESIAN_POINT('Ctrl Pts',(39.964809327259,-2.61193708735453,339.167369399777));
#28584=CARTESIAN_POINT('Ctrl Pts',(39.9570515157368,-2.49597883031505,339.240047303532));
#28585=CARTESIAN_POINT('Ctrl Pts',(39.9492937042146,-2.37686397691438,339.307957436375));
#28586=CARTESIAN_POINT('Ctrl Pts',(39.9415358926924,-2.25502352083456,339.370818228088));
#28587=CARTESIAN_POINT('Ctrl Pts',(39.9337839191694,-2.13327475356172,339.433631715061));
#28588=CARTESIAN_POINT('Ctrl Pts',(39.9260319456464,-2.00880481219777,339.491403245704));
#28589=CARTESIAN_POINT('Ctrl Pts',(39.9182799721234,-1.88207144757164,339.543895919664));
#28590=CARTESIAN_POINT('Ctrl Pts',(39.9105312815658,-1.75539175460049,339.596366362945));
#28591=CARTESIAN_POINT('Ctrl Pts',(39.9027825910081,-1.62645090524884,339.643562246726));
#28592=CARTESIAN_POINT('Ctrl Pts',(39.8950339004505,-1.49572870015399,339.685293877446));
#28593=CARTESIAN_POINT('Ctrl Pts',(39.8872868220727,-1.3650336929059,339.727016825552));
#28594=CARTESIAN_POINT('Ctrl Pts',(39.8795397436949,-1.23255843924232,339.76327766314));
#28595=CARTESIAN_POINT('Ctrl Pts',(39.8717926653171,-1.09879967709113,339.793935995831));
#28596=CARTESIAN_POINT('Ctrl Pts',(39.8640455220113,-0.965039793912857,
339.824594585468));
#28597=CARTESIAN_POINT('Ctrl Pts',(39.8562983787055,-0.829996761785789,
339.849650489228));
#28598=CARTESIAN_POINT('Ctrl Pts',(39.8485512353997,-0.694178946508504,
339.869014135605));
#28599=CARTESIAN_POINT('Ctrl Pts',(39.8408023503716,-0.558330596502665,
339.888382135341));
#28600=CARTESIAN_POINT('Ctrl Pts',(39.8330534653435,-0.42170750361822,339.902055275995));
#28601=CARTESIAN_POINT('Ctrl Pts',(39.8253045803154,-0.284824217742129,
339.909995746178));
#28602=CARTESIAN_POINT('Ctrl Pts',(39.8175474705407,-0.14779564253214,339.917944644458));
#28603=CARTESIAN_POINT('Ctrl Pts',(39.809790360766,-0.0105067134865973,
339.920148694805));
#28604=CARTESIAN_POINT('Ctrl Pts',(39.8020332509913,0.126526390383609,339.916622228221));
#28605=CARTESIAN_POINT('Ctrl Pts',(39.7942719960651,0.263632720363148,339.913093877206));
#28606=CARTESIAN_POINT('Ctrl Pts',(39.7865107411389,0.400482562986988,339.903828933928));
#28607=CARTESIAN_POINT('Ctrl Pts',(39.7787494862127,0.536564787416517,339.888893667427));
#28608=CARTESIAN_POINT('Ctrl Pts',(39.7709758158081,0.67286469905604,339.873934509366));
#28609=CARTESIAN_POINT('Ctrl Pts',(39.7632021454034,0.808394152096627,339.853286961097));
#28610=CARTESIAN_POINT('Ctrl Pts',(39.7554284749988,0.942651253067361,339.827068642312));
#28611=CARTESIAN_POINT('Ctrl Pts',(39.7480166708216,1.07065865368825,339.802070792574));
#28612=CARTESIAN_POINT('Ctrl Pts',(39.7406048666445,1.19750921239909,339.772009205777));
#28613=CARTESIAN_POINT('Ctrl Pts',(39.7331930624674,1.32278248097241,339.737027503671));
#28614=CARTESIAN_POINT('Ctrl Pts',(39.7254179836889,1.45419576560766,339.700331244139));
#28615=CARTESIAN_POINT('Ctrl Pts',(39.7176429049105,1.58428852553508,339.658104408384));
#28616=CARTESIAN_POINT('Ctrl Pts',(39.7098678261321,1.71255993317724,339.610457844702));
#28617=CARTESIAN_POINT('Ctrl Pts',(39.702102315083,1.84067349468632,339.56286991315));
#28618=CARTESIAN_POINT('Ctrl Pts',(39.694336804034,1.96696980052449,339.50987565851));
#28619=CARTESIAN_POINT('Ctrl Pts',(39.686571292985,2.09096080431581,339.451636325815));
#28620=CARTESIAN_POINT('Ctrl Pts',(39.6788134814628,2.21482887066563,339.393454737588));
#28621=CARTESIAN_POINT('Ctrl Pts',(39.6710556699406,2.33639583215662,339.330038585723));
#28622=CARTESIAN_POINT('Ctrl Pts',(39.6632978584184,2.45519167497269,339.261597928201));
#28623=CARTESIAN_POINT('Ctrl Pts',(39.6555458848953,2.57389812015029,339.193208774443));
#28624=CARTESIAN_POINT('Ctrl Pts',(39.6477939113723,2.68983726012588,339.11980283546));
#28625=CARTESIAN_POINT('Ctrl Pts',(39.6400419378492,2.80256216509931,339.041636843317));
#28626=CARTESIAN_POINT('Ctrl Pts',(39.6322932472916,2.91523933100809,338.963503954517));
#28627=CARTESIAN_POINT('Ctrl Pts',(39.624544556734,3.02470464876855,338.880615244278));
#28628=CARTESIAN_POINT('Ctrl Pts',(39.6167958661763,3.13053895336149,338.793271533121));
#28629=CARTESIAN_POINT('Ctrl Pts',(39.6090487877985,3.23635123824341,338.705945994552));
#28630=CARTESIAN_POINT('Ctrl Pts',(39.6013017094207,3.33853371134819,338.614167547376));
#28631=CARTESIAN_POINT('Ctrl Pts',(39.5935546310429,3.43669949865113,338.518277933659));
#28632=CARTESIAN_POINT('Ctrl Pts',(39.5858074877371,3.53486610867779,338.422387516294));
#28633=CARTESIAN_POINT('Ctrl Pts',(39.5780603444313,3.6290156861453,338.322386136794));
#28634=CARTESIAN_POINT('Ctrl Pts',(39.5703132011255,3.71879780256008,338.218652818521));
#28635=CARTESIAN_POINT('Ctrl Pts',(39.5625643160974,3.80860010390089,338.114896178796));
#28636=CARTESIAN_POINT('Ctrl Pts',(39.5548154310692,3.89403273457162,338.007406226236));
#28637=CARTESIAN_POINT('Ctrl Pts',(39.5470665460411,3.97478544569988,337.896595194906));
#28638=CARTESIAN_POINT('Ctrl Pts',(39.5393094362664,4.05562386859006,337.785666547602));
#28639=CARTESIAN_POINT('Ctrl Pts',(39.5315523264916,4.13177221869177,337.671410096348));
#28640=CARTESIAN_POINT('Ctrl Pts',(39.5237952167169,4.20296321316905,337.554267662413));
#28641=CARTESIAN_POINT('Ctrl Pts',(39.5160339617907,4.27419224983758,337.437062631306));
#28642=CARTESIAN_POINT('Ctrl Pts',(39.5082727068645,4.34045846366295,337.316968886651));
#28643=CARTESIAN_POINT('Ctrl Pts',(39.5005114519383,4.40154097946671,337.194452111251));
#28644=CARTESIAN_POINT('Ctrl Pts',(39.4927377815337,4.46272120738893,337.071739348939));
#28645=CARTESIAN_POINT('Ctrl Pts',(39.484964111129,4.51870100727224,336.946596167359));
#28646=CARTESIAN_POINT('Ctrl Pts',(39.4771904407244,4.56930768466818,336.819508270202));
#28647=CARTESIAN_POINT('Ctrl Pts',(39.4697786365474,4.61755860905538,336.698336345234));
#28648=CARTESIAN_POINT('Ctrl Pts',(39.4623668323704,4.66092529538337,336.57539695463));
#28649=CARTESIAN_POINT('Ctrl Pts',(39.4549550281934,4.69930098958318,336.451121384241));
#28650=CARTESIAN_POINT('Ctrl Pts',(39.447179949415,4.73955759087155,336.320754697949));
#28651=CARTESIAN_POINT('Ctrl Pts',(39.4394048706366,4.77444880093273,336.188505556916));
#28652=CARTESIAN_POINT('Ctrl Pts',(39.4316297918581,4.80379680792477,336.054855104112));
#28653=CARTESIAN_POINT('Ctrl Pts',(39.4238642808091,4.83310870032582,335.921369116699));
#28654=CARTESIAN_POINT('Ctrl Pts',(39.4160987697601,4.85689087898534,335.786485626711));
#28655=CARTESIAN_POINT('Ctrl Pts',(39.4083332587111,4.8750148283944,335.650702301698));
#28656=CARTESIAN_POINT('Ctrl Pts',(39.400575447189,4.89312080785479,335.515053606247));
#28657=CARTESIAN_POINT('Ctrl Pts',(39.3928176356667,4.90557967120106,335.37850723622));
#28658=CARTESIAN_POINT('Ctrl Pts',(39.3850598241446,4.91231370922472,335.241572110689));
#28659=CARTESIAN_POINT('Ctrl Pts',(39.3773078506216,4.91904267967125,335.104740033182));
#28660=CARTESIAN_POINT('Ctrl Pts',(39.3695558770986,4.92005538076119,334.967520171308));
#28661=CARTESIAN_POINT('Ctrl Pts',(39.3618039035756,4.9153258446041,334.830427290324));
#28662=CARTESIAN_POINT('Ctrl Pts',(39.354055213018,4.91059831140839,334.693392468256));
#28663=CARTESIAN_POINT('Ctrl Pts',(39.3463065224604,4.90013339117445,334.556484909947));
#28664=CARTESIAN_POINT('Ctrl Pts',(39.3385578319027,4.88395721605244,334.420219891451));
#28665=CARTESIAN_POINT('Ctrl Pts',(39.3308107535249,4.86778440651878,334.28398322403));
#28666=CARTESIAN_POINT('Ctrl Pts',(39.323063675147,4.84590275170732,334.148389218415));
#28667=CARTESIAN_POINT('Ctrl Pts',(39.3153165967692,4.81839027007874,334.01394814147));
#28668=CARTESIAN_POINT('Ctrl Pts',(39.3075694534634,4.79087755786903,333.879505937779));
#28669=CARTESIAN_POINT('Ctrl Pts',(39.2998223101577,4.75773400308046,333.746217064967));
#28670=CARTESIAN_POINT('Ctrl Pts',(39.2920751668518,4.71908869758066,333.614581317122));
#28671=CARTESIAN_POINT('Ctrl Pts',(39.2843262818238,4.68043470379588,333.482915974767));
#28672=CARTESIAN_POINT('Ctrl Pts',(39.2765773967957,4.6362766080701,333.352904871909));
#28673=CARTESIAN_POINT('Ctrl Pts',(39.2688285117676,4.58679317335638,333.22503198695));
#28674=CARTESIAN_POINT('Ctrl Pts',(39.2610714019929,4.53725721641367,333.097023376389));
#28675=CARTESIAN_POINT('Ctrl Pts',(39.2533142922182,4.48238477063109,332.971157882427));
#28676=CARTESIAN_POINT('Ctrl Pts',(39.2455571824434,4.4224027308611,332.847899363744));
#28677=CARTESIAN_POINT('Ctrl Pts',(39.2377959275173,4.36238863860695,332.72457497965));
#28678=CARTESIAN_POINT('Ctrl Pts',(39.2300346725911,4.29725969729425,332.603860690506));
#28679=CARTESIAN_POINT('Ctrl Pts',(39.2222734176649,4.22728798129583,332.486194242649));
#28680=CARTESIAN_POINT('Ctrl Pts',(39.2144997472603,4.15720433335545,332.368339566822));
#28681=CARTESIAN_POINT('Ctrl Pts',(39.2067260768556,4.0822626439893,332.253542802556));
#28682=CARTESIAN_POINT('Ctrl Pts',(39.198952406451,4.00277789691776,332.142212014434));
#28683=CARTESIAN_POINT('Ctrl Pts',(39.1915406022738,3.92699318394469,332.036063701282));
#28684=CARTESIAN_POINT('Ctrl Pts',(39.1841287980967,3.84707902993871,331.933066171042));
#28685=CARTESIAN_POINT('Ctrl Pts',(39.1767169939195,3.76334034162273,331.83354258901));
#28686=CARTESIAN_POINT('Ctrl Pts',(39.1689419151411,3.67549737074852,331.729141059758));
#28687=CARTESIAN_POINT('Ctrl Pts',(39.1611668363626,3.58316788246391,331.628232698179));
#28688=CARTESIAN_POINT('Ctrl Pts',(39.1533917575842,3.48666025596526,331.531227404114));
#28689=CARTESIAN_POINT('Ctrl Pts',(39.1456262465352,3.39027138824499,331.434341481238));
#28690=CARTESIAN_POINT('Ctrl Pts',(39.1378607354862,3.28971488539471,331.341349343787));
#28691=CARTESIAN_POINT('Ctrl Pts',(39.1300952244372,3.18533969955816,331.252628379661));
#28692=CARTESIAN_POINT('Ctrl Pts',(39.122337412915,3.08106800202204,331.16399538263));
#28693=CARTESIAN_POINT('Ctrl Pts',(39.1145796013928,2.97298545222309,331.079625382793));
#28694=CARTESIAN_POINT('Ctrl Pts',(39.1068217898706,2.86147795815404,330.999859132793));
#28695=CARTESIAN_POINT('Ctrl Pts',(39.0990698163476,2.75005437701114,330.920152909427));
#28696=CARTESIAN_POINT('Ctrl Pts',(39.0913178428247,2.63521129837364,330.845043766542));
#28697=CARTESIAN_POINT('Ctrl Pts',(39.0835658693017,2.51736754661055,330.774832110108));
#28698=CARTESIAN_POINT('Ctrl Pts',(39.0758171787441,2.39957370174583,330.704650188353));
#28699=CARTESIAN_POINT('Ctrl Pts',(39.0680684881864,2.27878204635426,330.639361827482));
#28700=CARTESIAN_POINT('Ctrl Pts',(39.0603197976288,2.15544002866688,330.579223897852));
#28701=CARTESIAN_POINT('Ctrl Pts',(39.052572719251,2.03212367331644,330.519098480421));
#28702=CARTESIAN_POINT('Ctrl Pts',(39.0448256408732,1.90625836223653,330.464121533956));
#28703=CARTESIAN_POINT('Ctrl Pts',(39.0370785624954,1.77831540998343,330.414503585748));
#28704=CARTESIAN_POINT('Ctrl Pts',(39.0293314191896,1.65037138544551,330.364885221694));
#28705=CARTESIAN_POINT('Ctrl Pts',(39.0215842758838,1.52035004943253,330.320626086811));
#28706=CARTESIAN_POINT('Ctrl Pts',(39.013837132578,1.38874154847184,330.28188809225));
#28707=CARTESIAN_POINT('Ctrl Pts',(39.0060882475499,1.25710345912512,330.243141388567));
#28708=CARTESIAN_POINT('Ctrl Pts',(38.9983393625217,1.12387786967725,330.209918405542));
#28709=CARTESIAN_POINT('Ctrl Pts',(38.9905904774936,0.989568506783285,330.182330726079));
#28710=CARTESIAN_POINT('Ctrl Pts',(38.9828333677189,0.855116586544422,330.154713764768));
#28711=CARTESIAN_POINT('Ctrl Pts',(38.9750762579442,0.719578978456182,330.132744134136));
#28712=CARTESIAN_POINT('Ctrl Pts',(38.9673191481695,0.583468537002301,330.116482054008));
#28713=CARTESIAN_POINT('Ctrl Pts',(38.9595578932433,0.447285362480382,330.100211283944));
#28714=CARTESIAN_POINT('Ctrl Pts',(38.9517966383171,0.310529134170466,330.089654171718));
#28715=CARTESIAN_POINT('Ctrl Pts',(38.944035383391,0.17371519736055,330.084818813848));
#28716=CARTESIAN_POINT('Ctrl Pts',(38.9362617129863,0.0366824028394827,
330.07997572098));
#28717=CARTESIAN_POINT('Ctrl Pts',(38.9284880425817,-0.100407893582374,
330.080872670198));
#28718=CARTESIAN_POINT('Ctrl Pts',(38.920714372177,-0.237042085926806,330.087465612131));
#28719=CARTESIAN_POINT('Ctrl Pts',(38.9133025679999,-0.367315923746237,
330.09375165103));
#28720=CARTESIAN_POINT('Ctrl Pts',(38.9058907638227,-0.4971748784866,330.105215294418));
#28721=CARTESIAN_POINT('Ctrl Pts',(38.8984789596456,-0.626182191032283,
330.121775023009));
#28722=CARTESIAN_POINT('Ctrl Pts',(38.8907038808672,-0.761512536258101,
330.139146393228));
#28723=CARTESIAN_POINT('Ctrl Pts',(38.8829288020887,-0.8963333142709,330.16218092512));
#28724=CARTESIAN_POINT('Ctrl Pts',(38.8751537233103,-1.03013294987281,330.190841116361));
#28725=CARTESIAN_POINT('Ctrl Pts',(38.8673882122612,-1.16376793650519,330.219466039412));
#28726=CARTESIAN_POINT('Ctrl Pts',(38.8596227012122,-1.29638390241144,330.253702766475));
#28727=CARTESIAN_POINT('Ctrl Pts',(38.8518571901632,-1.42747465602692,330.293462082496));
#28728=CARTESIAN_POINT('Ctrl Pts',(38.844099378641,-1.55843543277844,330.333181977039));
#28729=CARTESIAN_POINT('Ctrl Pts',(38.8363415671188,-1.68787363506793,330.378413450944));
#28730=CARTESIAN_POINT('Ctrl Pts',(38.8285837555966,-1.81529387977036,330.429016386753));
#28731=CARTESIAN_POINT('Ctrl Pts',(38.8208317820736,-1.94261823669775,330.479581242249));
#28732=CARTESIAN_POINT('Ctrl Pts',(38.8130798085506,-2.06792729687868,330.535509370169));
#28733=CARTESIAN_POINT('Ctrl Pts',(38.8053278350276,-2.19074179262632,330.596611139072));
#28734=CARTESIAN_POINT('Ctrl Pts',(38.7975791444699,-2.31350427636192,330.657687031341));
#28735=CARTESIAN_POINT('Ctrl Pts',(38.7898304539123,-2.43377394764012,330.723932033024));
#28736=CARTESIAN_POINT('Ctrl Pts',(38.7820817633547,-2.55109265878631,330.795108882648));
#28737=CARTESIAN_POINT('Ctrl Pts',(38.7743346849768,-2.66838696079509,330.866270923334));
#28738=CARTESIAN_POINT('Ctrl Pts',(38.766587606599,-2.78273118993459,330.942362568331));
#28739=CARTESIAN_POINT('Ctrl Pts',(38.7588405282211,-2.89369325396463,331.023101407572));
#28740=CARTESIAN_POINT('Ctrl Pts',(38.7510933849153,-3.00465624796379,331.103840923481));
#28741=CARTESIAN_POINT('Ctrl Pts',(38.7433462416095,-3.11223670425458,331.189227481345));
#28742=CARTESIAN_POINT('Ctrl Pts',(38.7355990983037,-3.21603322188358,331.278936525905));
#28743=CARTESIAN_POINT('Ctrl Pts',(38.7278502132756,-3.31985307517255,331.368665738963));
#28744=CARTESIAN_POINT('Ctrl Pts',(38.7201013282475,-3.41988700131146,331.462719116923));
#28745=CARTESIAN_POINT('Ctrl Pts',(38.7123524432195,-3.51576857245959,331.560733449207));
#28746=CARTESIAN_POINT('Ctrl Pts',(38.7045953334447,-3.6117519132985,331.658851814916));
#28747=CARTESIAN_POINT('Ctrl Pts',(38.69683822367,-3.70357382128163,331.760939253373));
#28748=CARTESIAN_POINT('Ctrl Pts',(38.6890811138953,-3.79090612128399,331.866597082705));
#28749=CARTESIAN_POINT('Ctrl Pts',(38.6813198589691,-3.87828508887506,331.972311372203));
#28750=CARTESIAN_POINT('Ctrl Pts',(38.6735586040429,-3.96116943198058,332.081599542963));
#28751=CARTESIAN_POINT('Ctrl Pts',(38.6657973491168,-4.0392734591617,332.194032611627));
#28752=CARTESIAN_POINT('Ctrl Pts',(38.6580236787121,-4.11750242733227,332.306645536559));
#28753=CARTESIAN_POINT('Ctrl Pts',(38.6502500083074,-4.19093558923302,332.422413082202));
#28754=CARTESIAN_POINT('Ctrl Pts',(38.6424763379028,-4.2593320452533,332.540879508691));
#28755=CARTESIAN_POINT('Ctrl Pts',(38.6350645337257,-4.32454462979014,332.653831294523));
#28756=CARTESIAN_POINT('Ctrl Pts',(38.6276527295487,-4.38517873921408,332.769236095203));
#28757=CARTESIAN_POINT('Ctrl Pts',(38.6202409253717,-4.44106656941066,332.886682515909));
#28758=CARTESIAN_POINT('Ctrl Pts',(38.6118318156202,-4.50447446398924,333.019932102386));
#28759=CARTESIAN_POINT('Ctrl Pts',(38.6034227058687,-4.56194910346594,333.156179451567));
#28760=CARTESIAN_POINT('Ctrl Pts',(38.5950135961173,-4.61322019579876,333.294895168157));
#28761=CARTESIAN_POINT('Ctrl Pts',(38.5866322854229,-4.66432179480058,333.433152314668));
#28762=CARTESIAN_POINT('Ctrl Pts',(38.5782509747286,-4.7092606479371,333.573861283209));
#28763=CARTESIAN_POINT('Ctrl Pts',(38.5698696640342,-4.74781433414765,333.716472785266));
#28764=CARTESIAN_POINT('Ctrl Pts',(38.5615052133412,-4.78629046504147,333.858797407357));
#28765=CARTESIAN_POINT('Ctrl Pts',(38.5531407626483,-4.81840695593296,334.003016657154));
#28766=CARTESIAN_POINT('Ctrl Pts',(38.5447763119554,-4.84398994818294,334.148563305699));
#28767=CARTESIAN_POINT('Ctrl Pts',(38.5364387881212,-4.86949058360599,334.293641410141));
#28768=CARTESIAN_POINT('Ctrl Pts',(38.5281012642869,-4.88849961290795,334.440038108003));
#28769=CARTESIAN_POINT('Ctrl Pts',(38.5197637404527,-4.90089360764275,334.587174481086));
#28770=CARTESIAN_POINT('Ctrl Pts',(38.5120212431428,-4.91240307649727,334.723810129204));
#28771=CARTESIAN_POINT('Ctrl Pts',(38.5042787458329,-4.918208425872,334.861083299193));
#28772=CARTESIAN_POINT('Ctrl Pts',(38.4965362485229,-4.91824977738391,334.998520215163));
#28773=CARTESIAN_POINT('',(41.9965362485248,-4.91824873401151,335.003528865855));
#28774=CARTESIAN_POINT('Ctrl Pts',(41.9965362484901,-4.91824873401107,335.003528866466));
#28775=CARTESIAN_POINT('Ctrl Pts',(41.984056611213,-4.91809120867879,335.223074937012));
#28776=CARTESIAN_POINT('Ctrl Pts',(41.971576973936,-4.9032326330616,335.442100836012));
#28777=CARTESIAN_POINT('Ctrl Pts',(41.9590973366589,-4.87388334896147,335.659123784441));
#28778=CARTESIAN_POINT('Ctrl Pts',(41.9513222578805,-4.85559812232357,335.794333685443));
#28779=CARTESIAN_POINT('Ctrl Pts',(41.9435471791021,-4.8316533057367,335.928995772172));
#28780=CARTESIAN_POINT('Ctrl Pts',(41.9357721003236,-4.80208985672172,336.062598734457));
#28781=CARTESIAN_POINT('Ctrl Pts',(41.9280065892746,-4.77256278741286,336.196037289792));
#28782=CARTESIAN_POINT('Ctrl Pts',(41.9202410782257,-4.73743092636431,336.328418935924));
#28783=CARTESIAN_POINT('Ctrl Pts',(41.9124755671766,-4.69678690627934,336.459238095549));
#28784=CARTESIAN_POINT('Ctrl Pts',(41.9047177556544,-4.65618318485865,336.589927547597));
#28785=CARTESIAN_POINT('Ctrl Pts',(41.8969599441322,-4.61007829592562,336.719057225286));
#28786=CARTESIAN_POINT('Ctrl Pts',(41.88920213261,-4.55861570040531,336.846132703388));
#28787=CARTESIAN_POINT('Ctrl Pts',(41.881450159087,-4.5071918321201,336.973112553163));
#28788=CARTESIAN_POINT('Ctrl Pts',(41.873698185564,-4.45041842856548,337.098040919456));
#28789=CARTESIAN_POINT('Ctrl Pts',(41.865946212041,-4.38848835464824,337.220439826615));
#28790=CARTESIAN_POINT('Ctrl Pts',(41.8581975214834,-4.32658450815407,337.342786897763));
#28791=CARTESIAN_POINT('Ctrl Pts',(41.8504488309257,-4.2595285109275,337.462606292326));
#28792=CARTESIAN_POINT('Ctrl Pts',(41.8427001403681,-4.18756071414259,337.579441475954));
#28793=CARTESIAN_POINT('Ctrl Pts',(41.8349530619903,-4.11560789085889,337.696252351045));
#28794=CARTESIAN_POINT('Ctrl Pts',(41.8272059836125,-4.03874550560012,337.810079917602));
#28795=CARTESIAN_POINT('Ctrl Pts',(41.8194589052346,-3.95725888108104,337.920494001125));
#28796=CARTESIAN_POINT('Ctrl Pts',(41.8117117619288,-3.87577157362567,338.030909010023));
#28797=CARTESIAN_POINT('Ctrl Pts',(41.803964618623,-3.7896601817132,338.137910164327));
#28798=CARTESIAN_POINT('Ctrl Pts',(41.7962174753172,-3.69925196494271,338.241098264843));
#28799=CARTESIAN_POINT('Ctrl Pts',(41.7884685902891,-3.60882342248567,338.344309564235));
#28800=CARTESIAN_POINT('Ctrl Pts',(41.780719705261,-3.51409639043736,338.443705810059));
#28801=CARTESIAN_POINT('Ctrl Pts',(41.7729708202329,-3.41543654656948,338.538923036583));
#28802=CARTESIAN_POINT('Ctrl Pts',(41.7652137104582,-3.31667198412384,338.634241327655));
#28803=CARTESIAN_POINT('Ctrl Pts',(41.7574566006834,-3.21396655294616,338.725371466923));
#28804=CARTESIAN_POINT('Ctrl Pts',(41.7496994909087,-3.10772114286859,338.811987980132));
#28805=CARTESIAN_POINT('Ctrl Pts',(41.7419382359825,-3.00141895864101,338.898650778435));
#28806=CARTESIAN_POINT('Ctrl Pts',(41.7341769810564,-2.89157333909619,338.980794910708));
#28807=CARTESIAN_POINT('Ctrl Pts',(41.7264157261303,-2.77861518785151,339.058137590119));
#28808=CARTESIAN_POINT('Ctrl Pts',(41.7186420557256,-2.66547634037781,339.135603992612));
#28809=CARTESIAN_POINT('Ctrl Pts',(41.7108683853209,-2.5492153432678,339.208253386567));
#28810=CARTESIAN_POINT('Ctrl Pts',(41.7030947149162,-2.43028955343579,339.275847956717));
#28811=CARTESIAN_POINT('Ctrl Pts',(41.6956829107391,-2.31689978773155,339.340295983365));
#28812=CARTESIAN_POINT('Ctrl Pts',(41.688271106562,-2.20108799401771,339.400149067519));
#28813=CARTESIAN_POINT('Ctrl Pts',(41.6808593023848,-2.08326669136225,339.45524218816));
#28814=CARTESIAN_POINT('Ctrl Pts',(41.6730842236064,-1.95967061569291,339.513035586757));
#28815=CARTESIAN_POINT('Ctrl Pts',(41.665309144828,-1.83347247986494,339.565773261686));
#28816=CARTESIAN_POINT('Ctrl Pts',(41.6575340660495,-1.70512441997229,339.61321295573));
#28817=CARTESIAN_POINT('Ctrl Pts',(41.6497685550005,-1.57693430053855,339.66059427221));
#28818=CARTESIAN_POINT('Ctrl Pts',(41.6420030439515,-1.44659988418907,339.702690445528));
#28819=CARTESIAN_POINT('Ctrl Pts',(41.6342375329025,-1.3145964505342,339.739305775611));
#28820=CARTESIAN_POINT('Ctrl Pts',(41.6264797213803,-1.18272389866784,339.775884801489));
#28821=CARTESIAN_POINT('Ctrl Pts',(41.6187219098581,-1.04918599693886,339.806993694837));
#28822=CARTESIAN_POINT('Ctrl Pts',(41.6109640983359,-0.914476153007197,
339.832485533148));
#28823=CARTESIAN_POINT('Ctrl Pts',(41.6032121248129,-0.779867682505355,
339.857958188042));
#28824=CARTESIAN_POINT('Ctrl Pts',(41.5954601512899,-0.644089407738613,
339.877822129175));
#28825=CARTESIAN_POINT('Ctrl Pts',(41.5877081777669,-0.5076476388997,339.891980880709));
#28826=CARTESIAN_POINT('Ctrl Pts',(41.5799594872093,-0.371263653230711,
339.906133636003));
#28827=CARTESIAN_POINT('Ctrl Pts',(41.5722107966516,-0.234217120336566,
339.914585966991));
#28828=CARTESIAN_POINT('Ctrl Pts',(41.564462106094,-0.0970220175030706,
339.917292933172));
#28829=CARTESIAN_POINT('Ctrl Pts',(41.5567150277162,0.0401445407434038,
339.919999336145));
#28830=CARTESIAN_POINT('Ctrl Pts',(41.5489679493384,0.177459216891762,339.916962744282));
#28831=CARTESIAN_POINT('Ctrl Pts',(41.5412208709606,0.314405863535913,339.908190299436));
#28832=CARTESIAN_POINT('Ctrl Pts',(41.5334737276547,0.451353657924867,339.899417781068));
#28833=CARTESIAN_POINT('Ctrl Pts',(41.5257265843489,0.587933026582659,339.884909338821));
#28834=CARTESIAN_POINT('Ctrl Pts',(41.5179794410431,0.723631175445326,339.864724142685));
#28835=CARTESIAN_POINT('Ctrl Pts',(41.510230556015,0.859359832132442,339.844534408489));
#28836=CARTESIAN_POINT('Ctrl Pts',(41.5024816709869,0.994206488249092,339.818665438297));
#28837=CARTESIAN_POINT('Ctrl Pts',(41.4947327859589,1.12766718802091,339.787227775609));
#28838=CARTESIAN_POINT('Ctrl Pts',(41.4869756761841,1.26126954435873,339.75575674466));
#28839=CARTESIAN_POINT('Ctrl Pts',(41.4792185664094,1.39348262469229,339.718705303863));
#28840=CARTESIAN_POINT('Ctrl Pts',(41.4714614566346,1.5238157862847,339.676234437234));
#28841=CARTESIAN_POINT('Ctrl Pts',(41.4637002017085,1.65421859375134,339.633740875531));
#28842=CARTESIAN_POINT('Ctrl Pts',(41.4559389467823,1.78273911472399,339.585822254005));
#28843=CARTESIAN_POINT('Ctrl Pts',(41.4481776918562,1.90890636105059,339.532687896518));
#28844=CARTESIAN_POINT('Ctrl Pts',(41.4404040214515,2.03527543385351,339.479468541376));
#28845=CARTESIAN_POINT('Ctrl Pts',(41.4326303510468,2.15928335572751,339.421016944276));
#28846=CARTESIAN_POINT('Ctrl Pts',(41.4248566806422,2.28048264067236,339.35758901092));
#28847=CARTESIAN_POINT('Ctrl Pts',(41.4174448764651,2.39604006974384,339.297113663122));
#28848=CARTESIAN_POINT('Ctrl Pts',(41.410033072288,2.50904421197558,339.232114993257));
#28849=CARTESIAN_POINT('Ctrl Pts',(41.402621268111,2.61913305993308,339.162850595069));
#28850=CARTESIAN_POINT('Ctrl Pts',(41.3948461893325,2.73461769026715,339.090191342397));
#28851=CARTESIAN_POINT('Ctrl Pts',(41.3870711105541,2.84725897876825,339.012608019652));
#28852=CARTESIAN_POINT('Ctrl Pts',(41.3792960317757,2.95660852938928,338.930349738438));
#28853=CARTESIAN_POINT('Ctrl Pts',(41.3715305207267,3.06582351842659,338.848192681277));
#28854=CARTESIAN_POINT('Ctrl Pts',(41.3637650096776,3.1717545199259,338.761372344866));
#28855=CARTESIAN_POINT('Ctrl Pts',(41.3559994986286,3.2739797644531,338.670182497431));
#28856=CARTESIAN_POINT('Ctrl Pts',(41.3482416871065,3.37610365235279,338.579083064996));
#28857=CARTESIAN_POINT('Ctrl Pts',(41.3404838755843,3.47452880547699,338.483623001744));
#28858=CARTESIAN_POINT('Ctrl Pts',(41.3327260640621,3.5688646623577,338.384137716505));
#28859=CARTESIAN_POINT('Ctrl Pts',(41.324974090539,3.66312952851454,338.284727297098));
#28860=CARTESIAN_POINT('Ctrl Pts',(41.317222117016,3.75331095582416,338.181297967484));
#28861=CARTESIAN_POINT('Ctrl Pts',(41.309470143493,3.83905382219862,338.074223286094));
#28862=CARTESIAN_POINT('Ctrl Pts',(41.3017214529354,3.92476037641827,337.967193950895));
#28863=CARTESIAN_POINT('Ctrl Pts',(41.2939727623778,4.00603186454649,337.856522638917));
#28864=CARTESIAN_POINT('Ctrl Pts',(41.2862240718202,4.08255235255462,337.742617244741));
#28865=CARTESIAN_POINT('Ctrl Pts',(41.2784769934423,4.159056919836,337.628735549534));
#28866=CARTESIAN_POINT('Ctrl Pts',(41.2707299150645,4.23081223533374,337.511621434784));
#28867=CARTESIAN_POINT('Ctrl Pts',(41.2629828366867,4.29754498780668,337.391712804723));
#28868=CARTESIAN_POINT('Ctrl Pts',(41.2552356933809,4.36427829956437,337.271803169713));
#28869=CARTESIAN_POINT('Ctrl Pts',(41.247488550075,4.42598877425816,337.149099314222));
#28870=CARTESIAN_POINT('Ctrl Pts',(41.2397414067692,4.48244866690289,337.024064477995));
#28871=CARTESIAN_POINT('Ctrl Pts',(41.2319925217411,4.53892125293017,336.899001531282));
#28872=CARTESIAN_POINT('Ctrl Pts',(41.2242436367131,4.59014074713045,336.771606917195));
#28873=CARTESIAN_POINT('Ctrl Pts',(41.216494751685,4.63592738850247,336.642364244324));
#28874=CARTESIAN_POINT('Ctrl Pts',(41.2087376419103,4.6817626282887,336.512984391944));
#28875=CARTESIAN_POINT('Ctrl Pts',(41.2009805321356,4.72215336541781,336.381752931423));
#28876=CARTESIAN_POINT('Ctrl Pts',(41.1932234223609,4.75696945984595,336.249169572393));
#28877=CARTESIAN_POINT('Ctrl Pts',(41.1854621674347,4.79180415888178,336.116515365055));
#28878=CARTESIAN_POINT('Ctrl Pts',(41.1777009125085,4.82105819614543,335.982508201426));
#28879=CARTESIAN_POINT('Ctrl Pts',(41.1699396575823,4.84465271782552,335.847657422645));
#28880=CARTESIAN_POINT('Ctrl Pts',(41.1621659871777,4.86828498305086,335.712590926566));
#28881=CARTESIAN_POINT('Ctrl Pts',(41.154392316773,4.88623959013899,335.576678506327));
#28882=CARTESIAN_POINT('Ctrl Pts',(41.1466186463684,4.8984895753013,335.44043494771));
#28883=CARTESIAN_POINT('Ctrl Pts',(41.1392068421913,4.91016932070711,335.310533559526));
#28884=CARTESIAN_POINT('Ctrl Pts',(41.1317950380142,4.91666357807027,335.180331455599));
#28885=CARTESIAN_POINT('Ctrl Pts',(41.1243832338371,4.91799306046915,335.050272454458));
#28886=CARTESIAN_POINT('Ctrl Pts',(41.1166081550587,4.91938770476073,334.913838874246));
#28887=CARTESIAN_POINT('Ctrl Pts',(41.1088330762803,4.91510289806022,334.777131623981));
#28888=CARTESIAN_POINT('Ctrl Pts',(41.1010579975018,4.90510547080146,334.64066257805));
#28889=CARTESIAN_POINT('Ctrl Pts',(41.0932924864528,4.8951203460134,334.504361465968));
#28890=CARTESIAN_POINT('Ctrl Pts',(41.0855269754038,4.87943661612563,334.368298361086));
#28891=CARTESIAN_POINT('Ctrl Pts',(41.0777614643548,4.85807307346464,334.232986913164));
#28892=CARTESIAN_POINT('Ctrl Pts',(41.0700036528325,4.83673071281841,334.097809626936));
#28893=CARTESIAN_POINT('Ctrl Pts',(41.0622458413103,4.80971980706881,333.963382898143));
#28894=CARTESIAN_POINT('Ctrl Pts',(41.0544880297881,4.77711105343428,333.830216667217));
#28895=CARTESIAN_POINT('Ctrl Pts',(41.0467360562651,4.74452683892095,333.697150648104));
#28896=CARTESIAN_POINT('Ctrl Pts',(41.0389840827421,4.70635325400689,333.565343616915));
#28897=CARTESIAN_POINT('Ctrl Pts',(41.0312321092191,4.6627122550075,333.435296357292));
#28898=CARTESIAN_POINT('Ctrl Pts',(41.0234834186615,4.61908973799709,333.305304172762));
#28899=CARTESIAN_POINT('Ctrl Pts',(41.0157347281038,4.5700045362693,333.177070647314));
#28900=CARTESIAN_POINT('Ctrl Pts',(41.0079860375462,4.51562868704753,333.051082191776));
#28901=CARTESIAN_POINT('Ctrl Pts',(41.0002389591684,4.46126415117542,332.925119949189));
#28902=CARTESIAN_POINT('Ctrl Pts',(40.9924918807906,4.40161131209717,332.801402206056));
#28903=CARTESIAN_POINT('Ctrl Pts',(40.9847448024127,4.33689050842846,332.680395770739));
#28904=CARTESIAN_POINT('Ctrl Pts',(40.9769976591069,4.27216916233707,332.559388321272));
#28905=CARTESIAN_POINT('Ctrl Pts',(40.9692505158011,4.20237995128564,332.441092569615));
#28906=CARTESIAN_POINT('Ctrl Pts',(40.9615033724953,4.12778917757917,332.325950716991));
#28907=CARTESIAN_POINT('Ctrl Pts',(40.9537544874672,4.05318163428327,332.210782978035));
#28908=CARTESIAN_POINT('Ctrl Pts',(40.9460056024392,3.97377059273798,332.098770877057));
#28909=CARTESIAN_POINT('Ctrl Pts',(40.9382567174111,3.88986545073272,331.990327287279));
#28910=CARTESIAN_POINT('Ctrl Pts',(40.9304996076363,3.80587125094262,331.881768594354));
#28911=CARTESIAN_POINT('Ctrl Pts',(40.9227424978616,3.71737366157023,331.776786288456));
#28912=CARTESIAN_POINT('Ctrl Pts',(40.9149853880868,3.62472247286212,331.67576022868));
#28913=CARTESIAN_POINT('Ctrl Pts',(40.9072241331606,3.53202177432123,331.574680183807));
#28914=CARTESIAN_POINT('Ctrl Pts',(40.8994628782345,3.43516332966786,331.477560874196));
#28915=CARTESIAN_POINT('Ctrl Pts',(40.8917016233083,3.33453278241015,331.384744243413));
#28916=CARTESIAN_POINT('Ctrl Pts',(40.8839279529037,3.23374125907223,331.291779136271));
#28917=CARTESIAN_POINT('Ctrl Pts',(40.876154282499,3.12916587345923,331.203130714881));
#28918=CARTESIAN_POINT('Ctrl Pts',(40.8683806120943,3.02122492826498,331.119100233795));
#28919=CARTESIAN_POINT('Ctrl Pts',(40.8609688079173,2.91830866003876,331.03898139182));
#28920=CARTESIAN_POINT('Ctrl Pts',(40.8535570037402,2.81233334840604,330.963060402824));
#28921=CARTESIAN_POINT('Ctrl Pts',(40.8461451995631,2.70368341887178,330.891560024411));
#28922=CARTESIAN_POINT('Ctrl Pts',(40.8383701207846,2.58970823263953,330.816555199463));
#28923=CARTESIAN_POINT('Ctrl Pts',(40.8305950420063,2.47242943460294,330.746178247451));
#28924=CARTESIAN_POINT('Ctrl Pts',(40.8228199632278,2.35225952089809,330.680734065973));
#28925=CARTESIAN_POINT('Ctrl Pts',(40.8150544521788,2.23223748392244,330.615370417727));
#28926=CARTESIAN_POINT('Ctrl Pts',(40.8072889411298,2.10933175007412,330.554927647437));
#28927=CARTESIAN_POINT('Ctrl Pts',(40.7995234300808,1.98398442799957,330.499667917592));
#28928=CARTESIAN_POINT('Ctrl Pts',(40.7917656185586,1.85876138815972,330.444462977929));
#28929=CARTESIAN_POINT('Ctrl Pts',(40.7840078070364,1.73110193306239,330.394431008472));
#28930=CARTESIAN_POINT('Ctrl Pts',(40.7762499955142,1.60147314081859,330.34978851645));
#28931=CARTESIAN_POINT('Ctrl Pts',(40.7684980219912,1.4719418983519,330.305179619319));
#28932=CARTESIAN_POINT('Ctrl Pts',(40.7607460484682,1.34044463664878,330.265952253609));
#28933=CARTESIAN_POINT('Ctrl Pts',(40.7529940749452,1.20746847291735,330.232274866416));
#28934=CARTESIAN_POINT('Ctrl Pts',(40.7452453843876,1.0745486246702,330.198611741616));
#28935=CARTESIAN_POINT('Ctrl Pts',(40.73749669383,0.940151498215772,330.170494016278));
#28936=CARTESIAN_POINT('Ctrl Pts',(40.7297480032724,0.804779226008882,330.148040245438));
#28937=CARTESIAN_POINT('Ctrl Pts',(40.7220009248945,0.669435119133876,330.125591146294));
#28938=CARTESIAN_POINT('Ctrl Pts',(40.7142538465167,0.533116655427259,330.108803721581));
#28939=CARTESIAN_POINT('Ctrl Pts',(40.7065067681389,0.396335621866165,330.097745300646));
#28940=CARTESIAN_POINT('Ctrl Pts',(40.6987596248331,0.259553441948266,330.086686787031));
#28941=CARTESIAN_POINT('Ctrl Pts',(40.6910124815273,0.122309074046436,330.081357404461));
#28942=CARTESIAN_POINT('Ctrl Pts',(40.6832653382215,-0.0148815139388311,
330.081772514102));
#28943=CARTESIAN_POINT('Ctrl Pts',(40.6755164531934,-0.15210294528073,330.082187717069));
#28944=CARTESIAN_POINT('Ctrl Pts',(40.6677675681653,-0.289270181850473,
330.088349980973));
#28945=CARTESIAN_POINT('Ctrl Pts',(40.6600186831373,-0.425868596852595,
330.100222556002));
#28946=CARTESIAN_POINT('Ctrl Pts',(40.6522615733625,-0.562611998823912,
330.112107732704));
#28947=CARTESIAN_POINT('Ctrl Pts',(40.6445044635878,-0.698784983152917,
330.129715294016));
#28948=CARTESIAN_POINT('Ctrl Pts',(40.6367473538131,-0.833878826649021,
330.152956657408));
#28949=CARTESIAN_POINT('Ctrl Pts',(40.6289860988869,-0.969044859975534,
330.176210440241));
#28950=CARTESIAN_POINT('Ctrl Pts',(40.6212248439607,-1.10313022151564,330.205103941599));
#28951=CARTESIAN_POINT('Ctrl Pts',(40.6134635890346,-1.23563866979703,330.239497910913));
#28952=CARTESIAN_POINT('Ctrl Pts',(40.6056899186299,-1.36835908841126,330.273946899369));
#28953=CARTESIAN_POINT('Ctrl Pts',(40.5979162482253,-1.49949717887832,330.313913824689));
#28954=CARTESIAN_POINT('Ctrl Pts',(40.5901425778206,-1.62857324222994,330.359209953338));
#28955=CARTESIAN_POINT('Ctrl Pts',(40.5827307736435,-1.75164078377967,330.402397536302));
#28956=CARTESIAN_POINT('Ctrl Pts',(40.5753189694664,-1.87283368511698,330.450429233247));
#28957=CARTESIAN_POINT('Ctrl Pts',(40.5679071652892,-1.99175658992211,330.503102319487));
#28958=CARTESIAN_POINT('Ctrl Pts',(40.5601320865108,-2.11650826054398,330.558357070588));
#28959=CARTESIAN_POINT('Ctrl Pts',(40.5523570077323,-2.23915602799083,330.618894306929));
#28960=CARTESIAN_POINT('Ctrl Pts',(40.5445819289539,-2.35922027203999,330.684532149292));
#28961=CARTESIAN_POINT('Ctrl Pts',(40.5368164179049,-2.47913676939318,330.750089220111));
#28962=CARTESIAN_POINT('Ctrl Pts',(40.5290509068559,-2.59647572933525,330.820734222574));
#28963=CARTESIAN_POINT('Ctrl Pts',(40.5212853958069,-2.71077744347913,330.896237249252));
#28964=CARTESIAN_POINT('Ctrl Pts',(40.5135275842847,-2.82496582714058,330.97166541446));
#28965=CARTESIAN_POINT('Ctrl Pts',(40.5057697727625,-2.93612263389326,331.051941804239));
#28966=CARTESIAN_POINT('Ctrl Pts',(40.4980119612403,-3.04381303542199,331.136790807127));
#28967=CARTESIAN_POINT('Ctrl Pts',(40.4902599877173,-3.15142239650851,331.22157595845));
#28968=CARTESIAN_POINT('Ctrl Pts',(40.4825080141942,-3.2555702388323,331.310926632736));
#28969=CARTESIAN_POINT('Ctrl Pts',(40.4747560406712,-3.35585130456456,331.404524359121));
#28970=CARTESIAN_POINT('Ctrl Pts',(40.4670073501136,-3.45608990120594,331.498082446814));
#28971=CARTESIAN_POINT('Ctrl Pts',(40.459258659556,-3.55246469313828,331.595883743111));
#28972=CARTESIAN_POINT('Ctrl Pts',(40.4515099689984,-3.64460425221766,331.697570151053));
#28973=CARTESIAN_POINT('Ctrl Pts',(40.4437628906205,-3.73672464089221,331.799235402288));
#28974=CARTESIAN_POINT('Ctrl Pts',(40.4360158122427,-3.82461128714093,331.904783867871));
#28975=CARTESIAN_POINT('Ctrl Pts',(40.4282687338649,-3.90793061498021,332.013821610988));
#28976=CARTESIAN_POINT('Ctrl Pts',(40.420521590559,-3.99125064111571,332.122860267947));
#28977=CARTESIAN_POINT('Ctrl Pts',(40.4127744472533,-4.07000303516805,332.235387950187));
#28978=CARTESIAN_POINT('Ctrl Pts',(40.4050273039475,-4.14389565976784,332.350979082103));
#28979=CARTESIAN_POINT('Ctrl Pts',(40.3972784189194,-4.21780489699833,332.466596201359));
#28980=CARTESIAN_POINT('Ctrl Pts',(40.3895295338913,-4.28685198017761,332.585277811514));
#28981=CARTESIAN_POINT('Ctrl Pts',(40.3817806488632,-4.35078931891849,332.706571264485));
#28982=CARTESIAN_POINT('Ctrl Pts',(40.3740235390885,-4.41479452141131,332.827993459581));
#28983=CARTESIAN_POINT('Ctrl Pts',(40.3662664293137,-4.47367896288824,332.952032688973));
#28984=CARTESIAN_POINT('Ctrl Pts',(40.358509319539,-4.52724183497792,333.07821321939));
#28985=CARTESIAN_POINT('Ctrl Pts',(40.3507480646129,-4.58083332935387,333.204461176649));
#28986=CARTESIAN_POINT('Ctrl Pts',(40.3429868096867,-4.62909745059222,333.332852349247));
#28987=CARTESIAN_POINT('Ctrl Pts',(40.3352255547605,-4.67188275273112,333.462894080672));
#28988=CARTESIAN_POINT('Ctrl Pts',(40.3274518843559,-4.71473649740974,333.593143836487));
#28989=CARTESIAN_POINT('Ctrl Pts',(40.3196782139512,-4.75209380270447,333.725049051062));
#28990=CARTESIAN_POINT('Ctrl Pts',(40.3119045435466,-4.78385378603542,333.858104200754));
#28991=CARTESIAN_POINT('Ctrl Pts',(40.3044927393695,-4.81413533450118,333.984965601217));
#28992=CARTESIAN_POINT('Ctrl Pts',(40.2970809351924,-4.83932888878897,334.112872004763));
#28993=CARTESIAN_POINT('Ctrl Pts',(40.2896691310154,-4.85939097442342,334.241381241866));
#28994=CARTESIAN_POINT('Ctrl Pts',(40.2767540041779,-4.89434931579393,334.465309594172));
#28995=CARTESIAN_POINT('Ctrl Pts',(40.2638388773405,-4.91383529265973,334.691713748575));
#28996=CARTESIAN_POINT('Ctrl Pts',(40.2509237505031,-4.91758155532653,334.918915419392));
#28997=CARTESIAN_POINT('Ctrl Pts',(40.2494612498321,-4.91800577970565,334.944643590722));
#28998=CARTESIAN_POINT('Ctrl Pts',(40.2479987491611,-4.91822820671533,334.970381944723));
#28999=CARTESIAN_POINT('Ctrl Pts',(40.2465362484901,-4.91824847584528,334.996128004963));
#29000=CARTESIAN_POINT('',(43.746536248449,-4.91824959557186,335.001994531842));
#29001=CARTESIAN_POINT('Ctrl Pts',(43.746536248449,-4.91824959557186,335.001994531842));
#29002=CARTESIAN_POINT('Ctrl Pts',(43.7381122937764,-4.91818896959446,335.15149010897));
#29003=CARTESIAN_POINT('Ctrl Pts',(43.7296883391039,-4.91130806957054,335.300771189963));
#29004=CARTESIAN_POINT('Ctrl Pts',(43.7212643844313,-4.89769029334711,335.449235854484));
#29005=CARTESIAN_POINT('Ctrl Pts',(43.7128031364178,-4.88401223043045,335.598357780773));
#29006=CARTESIAN_POINT('Ctrl Pts',(43.7043418884044,-4.8635375947404,335.746655781512));
#29007=CARTESIAN_POINT('Ctrl Pts',(43.6958806403909,-4.83640146697991,335.893534505598));
#29008=CARTESIAN_POINT('Ctrl Pts',(43.6874004131535,-4.80920447081761,336.040742689851));
#29009=CARTESIAN_POINT('Ctrl Pts',(43.6789201859162,-4.77531618448029,336.186524973221));
#29010=CARTESIAN_POINT('Ctrl Pts',(43.6704399586788,-4.73492171806959,336.330300487203));
#29011=CARTESIAN_POINT('Ctrl Pts',(43.6619313036429,-4.69439183951448,336.47455797192));
#29012=CARTESIAN_POINT('Ctrl Pts',(43.6534226486069,-4.64731221462689,336.616794965942));
#29013=CARTESIAN_POINT('Ctrl Pts',(43.644913993571,-4.59391736527239,336.756447068246));
#29014=CARTESIAN_POINT('Ctrl Pts',(43.6394511764814,-4.55963623690208,336.846107994424));
#29015=CARTESIAN_POINT('Ctrl Pts',(43.6339883593919,-4.52275290818965,336.934703882329));
#29016=CARTESIAN_POINT('Ctrl Pts',(43.6285255423024,-4.48333932707077,337.022090883427));
#29017=CARTESIAN_POINT('Ctrl Pts',(43.620750463524,-4.42724305053108,337.146466422022));
#29018=CARTESIAN_POINT('Ctrl Pts',(43.6129753847455,-4.36587862266312,337.268702418503));
#29019=CARTESIAN_POINT('Ctrl Pts',(43.6052003059671,-4.29943115870852,337.388320492318));
#29020=CARTESIAN_POINT('Ctrl Pts',(43.5974347949181,-4.23306546258865,337.507791368478));
#29021=CARTESIAN_POINT('Ctrl Pts',(43.5896692838691,-4.16162936403315,337.624650393445));
#29022=CARTESIAN_POINT('Ctrl Pts',(43.5819037728201,-4.08535587087988,337.738439422512));
#29023=CARTESIAN_POINT('Ctrl Pts',(43.5741459612979,-4.00915800311708,337.852115629425));
#29024=CARTESIAN_POINT('Ctrl Pts',(43.5663881497757,-3.92813250187994,337.962727575402));
#29025=CARTESIAN_POINT('Ctrl Pts',(43.5586303382535,-3.84255790991696,338.069842304001));
#29026=CARTESIAN_POINT('Ctrl Pts',(43.5508783647305,-3.75704771554815,338.17687642537));
#29027=CARTESIAN_POINT('Ctrl Pts',(43.5431263912075,-3.66699548742562,338.28041826361));
#29028=CARTESIAN_POINT('Ctrl Pts',(43.5353744176845,-3.57272242695035,338.380064721639));
#29029=CARTESIAN_POINT('Ctrl Pts',(43.5276257271268,-3.47848929117216,338.479668979333));
#29030=CARTESIAN_POINT('Ctrl Pts',(43.5198770365692,-3.38003914637162,338.575380854595));
#29031=CARTESIAN_POINT('Ctrl Pts',(43.5121283460116,-3.27773259059881,338.666831346957));
#29032=CARTESIAN_POINT('Ctrl Pts',(43.5043812676337,-3.17544732055942,338.75826281228));
#29033=CARTESIAN_POINT('Ctrl Pts',(43.4966341892559,-3.06930752673133,338.845434397915));
#29034=CARTESIAN_POINT('Ctrl Pts',(43.4888871108781,-2.95970939048294,338.928015196812));
#29035=CARTESIAN_POINT('Ctrl Pts',(43.4811399675723,-2.8501103356966,339.010596687816));
#29036=CARTESIAN_POINT('Ctrl Pts',(43.4733928242664,-2.73705319285481,339.088587080121));
#29037=CARTESIAN_POINT('Ctrl Pts',(43.4656456809606,-2.62096550144872,339.16169711809));
#29038=CARTESIAN_POINT('Ctrl Pts',(43.4578967959325,-2.50485171106531,339.234823592747));
#29039=CARTESIAN_POINT('Ctrl Pts',(43.4501479109045,-2.38570634702689,339.30306732149));
#29040=CARTESIAN_POINT('Ctrl Pts',(43.4423990258764,-2.26398371973685,339.366183777541));
#29041=CARTESIAN_POINT('Ctrl Pts',(43.4346419161017,-2.14213189479224,339.429367226052));
#29042=CARTESIAN_POINT('Ctrl Pts',(43.4268848063269,-2.01769768965781,339.487412350472));
#29043=CARTESIAN_POINT('Ctrl Pts',(43.4191276965522,-1.89115818335365,339.540121560931));
#29044=CARTESIAN_POINT('Ctrl Pts',(43.411366441626,-1.76455105838336,339.592858937507));
#29045=CARTESIAN_POINT('Ctrl Pts',(43.4036051866998,-1.63583675717992,339.640254583571));
#29046=CARTESIAN_POINT('Ctrl Pts',(43.3958439317737,-1.50550894813942,339.682160384862));
#29047=CARTESIAN_POINT('Ctrl Pts',(43.388070261369,-1.3749726570782,339.724133221778));
#29048=CARTESIAN_POINT('Ctrl Pts',(43.3802965909643,-1.24281807739595,339.760598560937));
#29049=CARTESIAN_POINT('Ctrl Pts',(43.3725229205596,-1.1095514027325,339.791458937233));
#29050=CARTESIAN_POINT('Ctrl Pts',(43.3651111163826,-0.982488323837292,
339.820882755588));
#29051=CARTESIAN_POINT('Ctrl Pts',(43.3576993122056,-0.854414638729723,
339.845211636134));
#29052=CARTESIAN_POINT('Ctrl Pts',(43.3502875080285,-0.725772800545157,
339.864405092556));
#29053=CARTESIAN_POINT('Ctrl Pts',(43.3425124292501,-0.59082584266642,339.884539277453));
#29054=CARTESIAN_POINT('Ctrl Pts',(43.3347373504716,-0.454827172425125,
339.899085532502));
#29055=CARTESIAN_POINT('Ctrl Pts',(43.3269622716932,-0.318279246714153,
339.907940645893));
#29056=CARTESIAN_POINT('Ctrl Pts',(43.3191967606442,-0.181899351918835,
339.916784862503));
#29057=CARTESIAN_POINT('Ctrl Pts',(43.3114312495952,-0.0449719328149411,
339.919951846985));
#29058=CARTESIAN_POINT('Ctrl Pts',(43.3036657385462,0.0919916530273213,
339.91738961221));
#29059=CARTESIAN_POINT('Ctrl Pts',(43.295907927024,0.228819439075556,339.914829917899));
#29060=CARTESIAN_POINT('Ctrl Pts',(43.2881501155018,0.365682932211432,339.906552316185));
#29061=CARTESIAN_POINT('Ctrl Pts',(43.2803923039797,0.502067314663267,339.892556742037));
#29062=CARTESIAN_POINT('Ctrl Pts',(43.2726403304567,0.638349063542123,339.878571700001));
#29063=CARTESIAN_POINT('Ctrl Pts',(43.2648883569337,0.774152032119386,339.858877290094));
#29064=CARTESIAN_POINT('Ctrl Pts',(43.2571363834107,0.908963426949346,339.833525478465));
#29065=CARTESIAN_POINT('Ctrl Pts',(43.2493876928531,1.04371772907356,339.808184403343));
#29066=CARTESIAN_POINT('Ctrl Pts',(43.2416390022954,1.17748090932436,339.777190763889));
#29067=CARTESIAN_POINT('Ctrl Pts',(43.2338903117378,1.30974752703994,339.74064810737));
#29068=CARTESIAN_POINT('Ctrl Pts',(43.22614323336,1.44198662558099,339.704113053857));
#29069=CARTESIAN_POINT('Ctrl Pts',(43.2183961549822,1.57272940440545,339.662031383725));
#29070=CARTESIAN_POINT('Ctrl Pts',(43.2106490766044,1.70148320024599,339.614557181548));
#29071=CARTESIAN_POINT('Ctrl Pts',(43.2029019332986,1.83023807516717,339.567082581493));
#29072=CARTESIAN_POINT('Ctrl Pts',(43.1951547899927,1.95700356711716,339.514215494473));
#29073=CARTESIAN_POINT('Ctrl Pts',(43.1874076466869,2.0813050687093,339.456158914745));
#29074=CARTESIAN_POINT('Ctrl Pts',(43.1796587616589,2.20563451591783,339.398089282666));
#29075=CARTESIAN_POINT('Ctrl Pts',(43.1719098766308,2.32749851637457,339.334828001639));
#29076=CARTESIAN_POINT('Ctrl Pts',(43.1641609916027,2.44644558886834,339.266624783504));
#29077=CARTESIAN_POINT('Ctrl Pts',(43.156403881828,2.56551891301413,339.198349173768));
#29078=CARTESIAN_POINT('Ctrl Pts',(43.1486467720533,2.68166878490923,339.125121343435));
#29079=CARTESIAN_POINT('Ctrl Pts',(43.1408896622786,2.79447087218239,339.047235551216));
#29080=CARTESIAN_POINT('Ctrl Pts',(43.1331284073524,2.9073332372842,338.969308139319));
#29081=CARTESIAN_POINT('Ctrl Pts',(43.1253671524262,3.01684394120711,338.886718041085));
#29082=CARTESIAN_POINT('Ctrl Pts',(43.1176058975001,3.1226112792139,338.799800239674));
#29083=CARTESIAN_POINT('Ctrl Pts',(43.1098322270954,3.22854781049201,338.712743398107));
#29084=CARTESIAN_POINT('Ctrl Pts',(43.1020585566908,3.33072871823893,338.621345280058));
#29085=CARTESIAN_POINT('Ctrl Pts',(43.0942848862861,3.42879811154415,338.525978810596));
#29086=CARTESIAN_POINT('Ctrl Pts',(43.086873082109,3.52230235099808,338.43505167323));
#29087=CARTESIAN_POINT('Ctrl Pts',(43.0794612779318,3.61206904556232,338.340517532343));
#29088=CARTESIAN_POINT('Ctrl Pts',(43.0720494737546,3.69782471265276,338.24272654675));
#29089=CARTESIAN_POINT('Ctrl Pts',(43.0642743949762,3.7877835204393,338.140142533649));
#29090=CARTESIAN_POINT('Ctrl Pts',(43.0564993161978,3.87361246071081,338.03365016371));
#29091=CARTESIAN_POINT('Ctrl Pts',(43.0487242374193,3.95495283219749,337.923616109819));
#29092=CARTESIAN_POINT('Ctrl Pts',(43.0409587263703,4.03619310917867,337.813717459837));
#29093=CARTESIAN_POINT('Ctrl Pts',(43.0331932153213,4.11295557736482,337.700286108918));
#29094=CARTESIAN_POINT('Ctrl Pts',(43.0254277042723,4.18491979474793,337.583723935336));
#29095=CARTESIAN_POINT('Ctrl Pts',(43.0176698927501,4.25681265940003,337.467277333488));
#29096=CARTESIAN_POINT('Ctrl Pts',(43.0099120812278,4.32391653688576,337.347706416999));
#29097=CARTESIAN_POINT('Ctrl Pts',(43.0021542697056,4.38595277508063,337.225444071924));
#29098=CARTESIAN_POINT('Ctrl Pts',(42.9944022961826,4.44794232903888,337.103273733141));
#29099=CARTESIAN_POINT('Ctrl Pts',(42.9866503226596,4.5048716582562,336.97841634437));
#29100=CARTESIAN_POINT('Ctrl Pts',(42.9788983491366,4.55650696021847,336.851331246423));
#29101=CARTESIAN_POINT('Ctrl Pts',(42.971149658579,4.60812039459969,336.72429996909));
#29102=CARTESIAN_POINT('Ctrl Pts',(42.9634009680213,4.65444411412603,336.595043220382));
#29103=CARTESIAN_POINT('Ctrl Pts',(42.9556522774637,4.695291670959,336.4640420715));
#29104=CARTESIAN_POINT('Ctrl Pts',(42.9479051990858,4.7361307291166,336.333068178502));
#29105=CARTESIAN_POINT('Ctrl Pts',(42.940158120708,4.7714957745706,336.20035098016));
#29106=CARTESIAN_POINT('Ctrl Pts',(42.9324110423302,4.80124977196343,336.066388151529));
#29107=CARTESIAN_POINT('Ctrl Pts',(42.9246638990244,4.83100401872342,335.93242420016));
#29108=CARTESIAN_POINT('Ctrl Pts',(42.9169167557186,4.85514703887497,335.797214979257));
#29109=CARTESIAN_POINT('Ctrl Pts',(42.9091696124127,4.87359269732948,335.661269448135));
#29110=CARTESIAN_POINT('Ctrl Pts',(42.9014207273846,4.89204250275962,335.525293353572));
#29111=CARTESIAN_POINT('Ctrl Pts',(42.8936718423565,4.90479234512532,335.388581006637));
#29112=CARTESIAN_POINT('Ctrl Pts',(42.8859229573284,4.91180789005123,335.251647200919));
#29113=CARTESIAN_POINT('Ctrl Pts',(42.8781658475537,4.91883088134902,335.114568052245));
#29114=CARTESIAN_POINT('Ctrl Pts',(42.8704087377789,4.92010739693597,334.977267366215));
#29115=CARTESIAN_POINT('Ctrl Pts',(42.8626516280042,4.91565525464364,334.840261213244));
#29116=CARTESIAN_POINT('Ctrl Pts',(42.854890373078,4.91120073326881,334.703181848565));
#29117=CARTESIAN_POINT('Ctrl Pts',(42.8471291181519,4.90101148329646,334.566397720154));
#29118=CARTESIAN_POINT('Ctrl Pts',(42.8393678632257,4.88515722530405,334.430419499491));
#29119=CARTESIAN_POINT('Ctrl Pts',(42.831594192821,4.86927760566573,334.29422375799));
#29120=CARTESIAN_POINT('Ctrl Pts',(42.8238205224164,4.84771493062566,334.158836886633));
#29121=CARTESIAN_POINT('Ctrl Pts',(42.8160468520117,4.82059020783828,334.02475997283));
#29122=CARTESIAN_POINT('Ctrl Pts',(42.8086350478347,4.79472814742274,333.896924371624));
#29123=CARTESIAN_POINT('Ctrl Pts',(42.8012232436577,4.76381028079485,333.770279795078));
#29124=CARTESIAN_POINT('Ctrl Pts',(42.7938114394807,4.7279830668526,333.645245711557));
#29125=CARTESIAN_POINT('Ctrl Pts',(42.7860363607022,4.69039985443093,333.514083335144));
#29126=CARTESIAN_POINT('Ctrl Pts',(42.7782612819238,4.64729511307846,333.384278816285));
#29127=CARTESIAN_POINT('Ctrl Pts',(42.7704862031454,4.59878307200934,333.256332222268));
#29128=CARTESIAN_POINT('Ctrl Pts',(42.7627206920964,4.55033072809519,333.128543074681));
#29129=CARTESIAN_POINT('Ctrl Pts',(42.7549551810473,4.49648446132126,333.002607664856));
#29130=CARTESIAN_POINT('Ctrl Pts',(42.7471896699983,4.43740881014279,332.879012938708));
#29131=CARTESIAN_POINT('Ctrl Pts',(42.7394318584762,4.37839173264449,332.755540757091));
#29132=CARTESIAN_POINT('Ctrl Pts',(42.7316740469539,4.31415575656308,332.634404991025));
#29133=CARTESIAN_POINT('Ctrl Pts',(42.7239162354317,4.244914110363,332.516074224511));
#29134=CARTESIAN_POINT('Ctrl Pts',(42.7161642619087,4.17572457069747,332.39783250565));
#29135=CARTESIAN_POINT('Ctrl Pts',(42.7084122883858,4.10153705540764,332.282391920797));
#29136=CARTESIAN_POINT('Ctrl Pts',(42.7006603148628,4.02261131002727,332.170197655146));
#29137=CARTESIAN_POINT('Ctrl Pts',(42.6929116243052,3.94371898974692,332.058050903833));
#29138=CARTESIAN_POINT('Ctrl Pts',(42.6851629337476,3.86009265487649,331.949148056333));
#29139=CARTESIAN_POINT('Ctrl Pts',(42.67741424319,3.77203595083023,331.843906235844));
#29140=CARTESIAN_POINT('Ctrl Pts',(42.6696671648122,3.68399756771671,331.738686311795));
#29141=CARTESIAN_POINT('Ctrl Pts',(42.6619200864343,3.5915308995744,331.637126199258));
#29142=CARTESIAN_POINT('Ctrl Pts',(42.6541730080565,3.49498029428049,331.539610454719));
#29143=CARTESIAN_POINT('Ctrl Pts',(42.6464258647507,3.39842887979951,331.442093892904));
#29144=CARTESIAN_POINT('Ctrl Pts',(42.6386787214448,3.29779373490988,331.348622044455));
#29145=CARTESIAN_POINT('Ctrl Pts',(42.630931578139,3.19345624172046,331.259542769297));
#29146=CARTESIAN_POINT('Ctrl Pts',(42.6231826931109,3.08909529124744,331.170443467227));
#29147=CARTESIAN_POINT('Ctrl Pts',(42.6154338080829,2.98103063337027,331.085738957296));
#29148=CARTESIAN_POINT('Ctrl Pts',(42.6076849230548,2.86967658869894,331.005736696364));
#29149=CARTESIAN_POINT('Ctrl Pts',(42.59992781328,2.75820435169409,330.925649520205));
#29150=CARTESIAN_POINT('Ctrl Pts',(42.5921707035053,2.64343607146026,330.850274791492));
#29151=CARTESIAN_POINT('Ctrl Pts',(42.5844135937306,2.52581536487079,330.779876802144));
#29152=CARTESIAN_POINT('Ctrl Pts',(42.5766523388044,2.40813180553642,330.709441194361));
#29153=CARTESIAN_POINT('Ctrl Pts',(42.5688910838783,2.2875931259754,330.643987811486));
#29154=CARTESIAN_POINT('Ctrl Pts',(42.5611298289521,2.16466649053501,330.583734377638));
#29155=CARTESIAN_POINT('Ctrl Pts',(42.5533561585475,2.04154321253977,330.523384557933));
#29156=CARTESIAN_POINT('Ctrl Pts',(42.5455824881428,1.91602470333266,330.468251466804));
#29157=CARTESIAN_POINT('Ctrl Pts',(42.5378088177382,1.78859782219465,330.418504513487));
#29158=CARTESIAN_POINT('Ctrl Pts',(42.530397013561,1.66710269302973,330.371073292814));
#29159=CARTESIAN_POINT('Ctrl Pts',(42.5229852093839,1.54387313506706,330.328538139231));
#29160=CARTESIAN_POINT('Ctrl Pts',(42.5155734052068,1.4193411455178,330.291002890727));
#29161=CARTESIAN_POINT('Ctrl Pts',(42.5077983264283,1.28870547219991,330.251627927883));
#29162=CARTESIAN_POINT('Ctrl Pts',(42.5000232476499,1.1562236341376,330.217630951149));
#29163=CARTESIAN_POINT('Ctrl Pts',(42.4922481688714,1.02237796456516,330.189186517846));
#29164=CARTESIAN_POINT('Ctrl Pts',(42.4844826578224,0.888697000610158,330.16077708723));
#29165=CARTESIAN_POINT('Ctrl Pts',(42.4767171467734,0.753655923124875,330.137906685292));
#29166=CARTESIAN_POINT('Ctrl Pts',(42.4689516357244,0.617753256515989,330.120700462509));
#29167=CARTESIAN_POINT('Ctrl Pts',(42.4611938242022,0.481985337796808,330.103511299746));
#29168=CARTESIAN_POINT('Ctrl Pts',(42.45343601268,0.345357915276657,330.09197518866));
#29169=CARTESIAN_POINT('Ctrl Pts',(42.4456782011578,0.208380421394342,330.086166398576));
#29170=CARTESIAN_POINT('Ctrl Pts',(42.4379262276348,0.071506007420166,330.080361979792));
#29171=CARTESIAN_POINT('Ctrl Pts',(42.4301742541118,-0.0657175646012655,
330.080276319677));
#29172=CARTESIAN_POINT('Ctrl Pts',(42.4224222805888,-0.202775365730806,
330.085931907925));
#29173=CARTESIAN_POINT('Ctrl Pts',(42.4146735900312,-0.339775122800384,
330.091585101027));
#29174=CARTESIAN_POINT('Ctrl Pts',(42.4069248994735,-0.476608858879873,
330.102974690484));
#29175=CARTESIAN_POINT('Ctrl Pts',(42.3991762089159,-0.612761486217139,
330.120071063682));
#29176=CARTESIAN_POINT('Ctrl Pts',(42.3914291305381,-0.748885785863119,
330.137163879838));
#29177=CARTESIAN_POINT('Ctrl Pts',(42.3836820521602,-0.884328871053551,
330.159961069357));
#29178=CARTESIAN_POINT('Ctrl Pts',(42.3759349737824,-1.01858101364081,330.188381168344));
#29179=CARTESIAN_POINT('Ctrl Pts',(42.3681878304766,-1.15283428139015,330.216801505518));
#29180=CARTESIAN_POINT('Ctrl Pts',(42.3604406871708,-1.28589620422812,330.250844765203));
#29181=CARTESIAN_POINT('Ctrl Pts',(42.352693543865,-1.41726787158047,330.290378482013));
#29182=CARTESIAN_POINT('Ctrl Pts',(42.3449446588369,-1.54866907407275,330.329921086842));
#29183=CARTESIAN_POINT('Ctrl Pts',(42.3371957738088,-1.67837889069072,330.374956492442));
#29184=CARTESIAN_POINT('Ctrl Pts',(42.3294468887807,-1.80591456174752,330.425302670321));
#29185=CARTESIAN_POINT('Ctrl Pts',(42.321689779006,-1.93358560048344,330.475702286154));
#29186=CARTESIAN_POINT('Ctrl Pts',(42.3139326692312,-2.05907751974478,330.531423790769));
#29187=CARTESIAN_POINT('Ctrl Pts',(42.3061755594565,-2.18192800427329,330.592237160796));
#29188=CARTESIAN_POINT('Ctrl Pts',(42.2984143045303,-2.30484413617248,330.653083027543));
#29189=CARTESIAN_POINT('Ctrl Pts',(42.2906530496042,-2.42511567823696,330.719025993578));
#29190=CARTESIAN_POINT('Ctrl Pts',(42.2828917946781,-2.5423067321758,330.789791033448));
#29191=CARTESIAN_POINT('Ctrl Pts',(42.2751181242734,-2.65968525360861,330.86066927432));
#29192=CARTESIAN_POINT('Ctrl Pts',(42.2673444538687,-2.77397311373386,330.936384787387));
#29193=CARTESIAN_POINT('Ctrl Pts',(42.259570783464,-2.88476438522012,331.016619839349));
#29194=CARTESIAN_POINT('Ctrl Pts',(42.252158979287,-2.99039829636355,331.093119930339));
#29195=CARTESIAN_POINT('Ctrl Pts',(42.2447471751099,-3.09285359918245,331.173728082346));
#29196=CARTESIAN_POINT('Ctrl Pts',(42.2373353709328,-3.19180919561692,331.258137212393));
#29197=CARTESIAN_POINT('Ctrl Pts',(42.2296717060472,-3.2941274047213,331.345414651262));
#29198=CARTESIAN_POINT('Ctrl Pts',(42.2220080411616,-3.39304721518895,331.437049180769));
#29199=CARTESIAN_POINT('Ctrl Pts',(42.214344376276,-3.48816669397042,331.532742268366));
#29200=CARTESIAN_POINT('Ctrl Pts',(42.2066902036045,-3.58316835778084,331.62831683052));
#29201=CARTESIAN_POINT('Ctrl Pts',(42.199036030933,-3.67437876941371,331.727939671103));
#29202=CARTESIAN_POINT('Ctrl Pts',(42.1913818582615,-3.76142826102061,331.831271469549));
#29203=CARTESIAN_POINT('Ctrl Pts',(42.1837352099999,-3.84839217890307,331.934501688));
#29204=CARTESIAN_POINT('Ctrl Pts',(42.1760885617383,-3.93120305480914,332.041433305814));
#29205=CARTESIAN_POINT('Ctrl Pts',(42.1684419134768,-4.00952774931863,332.151689923842));
#29206=CARTESIAN_POINT('Ctrl Pts',(42.1608009633331,-4.0877940779504,332.26186438101));
#29207=CARTESIAN_POINT('Ctrl Pts',(42.1531600131894,-4.16158064466773,332.375358580815));
#29208=CARTESIAN_POINT('Ctrl Pts',(42.1455190630456,-4.23059468085973,332.491763227129));
#29209=CARTESIAN_POINT('Ctrl Pts',(42.1378811123916,-4.29958162527869,332.608122178271));
#29210=CARTESIAN_POINT('Ctrl Pts',(42.1302431617375,-4.36379955897432,332.727388958204));
#29211=CARTESIAN_POINT('Ctrl Pts',(42.1226052110834,-4.4229993518083,332.849125806468));
#29212=CARTESIAN_POINT('Ctrl Pts',(42.1149684949439,-4.48218957623682,332.970842978522));
#29213=CARTESIAN_POINT('Ctrl Pts',(42.1073317788044,-4.53636309716481,333.095029062353));
#29214=CARTESIAN_POINT('Ctrl Pts',(42.0996950626649,-4.58531728162552,333.221222754439));
#29215=CARTESIAN_POINT('Ctrl Pts',(42.0920578173362,-4.63427485838587,333.347425191167));
#29216=CARTESIAN_POINT('Ctrl Pts',(42.0844205720074,-4.67801223514881,333.47563513653));
#29217=CARTESIAN_POINT('Ctrl Pts',(42.0767833266787,-4.71637556484622,333.605372955295));
#29218=CARTESIAN_POINT('Ctrl Pts',(42.0691402362242,-4.75476825571721,333.735210068221));
#29219=CARTESIAN_POINT('Ctrl Pts',(42.0614971457696,-4.78777857274076,333.866577002474));
#29220=CARTESIAN_POINT('Ctrl Pts',(42.0538540553152,-4.81530301176027,333.998980535937));
#29221=CARTESIAN_POINT('Ctrl Pts',(42.0462076894455,-4.84283924626572,334.131440810394));
#29222=CARTESIAN_POINT('Ctrl Pts',(42.0385613235758,-4.86488485507018,334.264938171483));
#29223=CARTESIAN_POINT('Ctrl Pts',(42.0309149577061,-4.88138798731653,334.39897223044));
#29224=CARTESIAN_POINT('Ctrl Pts',(42.0232593186771,-4.89791113379928,334.533168839713));
#29225=CARTESIAN_POINT('Ctrl Pts',(42.0156036796482,-4.90887835139367,334.667903045344));
#29226=CARTESIAN_POINT('Ctrl Pts',(42.0079480406192,-4.91428985496865,334.802672141216));
#29227=CARTESIAN_POINT('Ctrl Pts',(42.0041441099211,-4.91697872058704,334.869636152843));
#29228=CARTESIAN_POINT('Ctrl Pts',(42.000340179223,-4.918296749457,334.936608808896));
#29229=CARTESIAN_POINT('Ctrl Pts',(41.9965362485248,-4.91824873401151,335.003528865855));
#29230=CARTESIAN_POINT('',(45.4965362485242,-4.91824806876705,334.995641494621));
#29231=CARTESIAN_POINT('Ctrl Pts',(45.4965362484901,-4.91824806876759,334.995641495223));
#29232=CARTESIAN_POINT('Ctrl Pts',(45.4888448922254,-4.91836861593767,335.131669999676));
#29233=CARTESIAN_POINT('Ctrl Pts',(45.4811535359606,-4.91284152150253,335.267811737524));
#29234=CARTESIAN_POINT('Ctrl Pts',(45.4734621796958,-4.90166545359971,335.403557732533));
#29235=CARTESIAN_POINT('Ctrl Pts',(45.4657736941497,-4.89049355704787,335.539253061763));
#29236=CARTESIAN_POINT('Ctrl Pts',(45.4580852086035,-4.87367691054027,335.674552546379));
#29237=CARTESIAN_POINT('Ctrl Pts',(45.4503967230574,-4.85126624931149,335.808949220156));
#29238=CARTESIAN_POINT('Ctrl Pts',(45.4427095113432,-4.82885930109164,335.943323627029));
#29239=CARTESIAN_POINT('Ctrl Pts',(45.435022299629,-4.80086024643141,336.07679512861));
#29240=CARTESIAN_POINT('Ctrl Pts',(45.4273350879148,-4.76737138886389,336.208864385753));
#29241=CARTESIAN_POINT('Ctrl Pts',(45.4196474224994,-4.7338805547756,336.340941437657));
#29242=CARTESIAN_POINT('Ctrl Pts',(45.411959757084,-4.69489937097439,336.471615695214));
#29243=CARTESIAN_POINT('Ctrl Pts',(45.4042720916686,-4.65058059448133,336.600400948742));
#29244=CARTESIAN_POINT('Ctrl Pts',(45.3965822449971,-4.60624924322079,336.729222743094));
#29245=CARTESIAN_POINT('Ctrl Pts',(45.3888923983255,-4.5565774161553,336.856154091651));
#29246=CARTESIAN_POINT('Ctrl Pts',(45.381202551654,-4.50176660731064,336.980727259317));
#29247=CARTESIAN_POINT('Ctrl Pts',(45.3735042940699,-4.44689584812681,337.105436681197));
#29248=CARTESIAN_POINT('Ctrl Pts',(45.3658060364859,-4.38687504434181,337.227782408036));
#29249=CARTESIAN_POINT('Ctrl Pts',(45.3581077789019,-4.32195257877653,337.347319528591));
#29250=CARTESIAN_POINT('Ctrl Pts',(45.3504048901709,-4.25699105690859,337.46692856074));
#29251=CARTESIAN_POINT('Ctrl Pts',(45.3427020014398,-4.18712220483497,337.583725281629));
#29252=CARTESIAN_POINT('Ctrl Pts',(45.3349991127089,-4.1126379799387,337.697293441297));
#29253=CARTESIAN_POINT('Ctrl Pts',(45.327284537618,-4.03804075205248,337.811033899753));
#29254=CARTESIAN_POINT('Ctrl Pts',(45.3195699625271,-3.95881440009591,337.9215356939));
#29255=CARTESIAN_POINT('Ctrl Pts',(45.3118553874362,-3.87529174763549,338.028414920913));
#29256=CARTESIAN_POINT('Ctrl Pts',(45.3072215076062,-3.82512256397624,338.092613595301));
#29257=CARTESIAN_POINT('Ctrl Pts',(45.3025876277762,-3.77340402202431,338.155505931274));
#29258=CARTESIAN_POINT('Ctrl Pts',(45.2979537479462,-3.72021445435332,338.217015305547));
#29259=CARTESIAN_POINT('Ctrl Pts',(45.2901786691677,-3.63096892058864,338.320220448564));
#29260=CARTESIAN_POINT('Ctrl Pts',(45.2824035903893,-3.53728447553205,338.419872124906));
#29261=CARTESIAN_POINT('Ctrl Pts',(45.2746285116109,-3.43947500843542,338.515564638696));
#29262=CARTESIAN_POINT('Ctrl Pts',(45.2668630005619,-3.34178590211491,338.611139396755));
#29263=CARTESIAN_POINT('Ctrl Pts',(45.2590974895128,-3.23998215046829,338.702764415412));
#29264=CARTESIAN_POINT('Ctrl Pts',(45.2513319784638,-3.13441777271877,338.790067055946));
#29265=CARTESIAN_POINT('Ctrl Pts',(45.2435741669416,-3.0289580623572,338.877283135657));
#29266=CARTESIAN_POINT('Ctrl Pts',(45.2358163554194,-2.91974544543276,338.960185118432));
#29267=CARTESIAN_POINT('Ctrl Pts',(45.2280585438972,-2.80717039866113,339.038437496778));
#29268=CARTESIAN_POINT('Ctrl Pts',(45.2203065703742,-2.69468006818201,339.116630987728));
#29269=CARTESIAN_POINT('Ctrl Pts',(45.2125545968513,-2.57883266402352,339.190181616588));
#29270=CARTESIAN_POINT('Ctrl Pts',(45.2048026233282,-2.46005103114451,339.258794663595));
#29271=CARTESIAN_POINT('Ctrl Pts',(45.1970539327706,-2.3413197023577,339.327378652935));
#29272=CARTESIAN_POINT('Ctrl Pts',(45.189305242213,-2.21965695414906,339.391029024307));
#29273=CARTESIAN_POINT('Ctrl Pts',(45.1815565516554,-2.09551366451193,339.449494976325));
#29274=CARTESIAN_POINT('Ctrl Pts',(45.1738094732776,-1.97139620392307,339.507948764014));
#29275=CARTESIAN_POINT('Ctrl Pts',(45.1660623948997,-1.84479958185818,339.56122011145));
#29276=CARTESIAN_POINT('Ctrl Pts',(45.1583153165219,-1.71619791431085,339.609104878544));
#29277=CARTESIAN_POINT('Ctrl Pts',(45.150568173216,-1.58759516895751,339.656990046958));
#29278=CARTESIAN_POINT('Ctrl Pts',(45.1428210299102,-1.45698771090967,339.699488408594));
#29279=CARTESIAN_POINT('Ctrl Pts',(45.1350738866044,-1.32486782955475,339.736444689502));
#29280=CARTESIAN_POINT('Ctrl Pts',(45.1273250015763,-1.19271824484533,339.773409278967));
#29281=CARTESIAN_POINT('Ctrl Pts',(45.1195761165482,-1.05905593656923,339.804829203077));
#29282=CARTESIAN_POINT('Ctrl Pts',(45.1118272315201,-0.924386093011183,
339.830599695022));
#29283=CARTESIAN_POINT('Ctrl Pts',(45.1040701217454,-0.789573309490155,
339.856397540034));
#29284=CARTESIAN_POINT('Ctrl Pts',(45.0963130119706,-0.653751238958404,
339.876533900998));
#29285=CARTESIAN_POINT('Ctrl Pts',(45.0885559021959,-0.517433502723694,
339.890955492821));
#29286=CARTESIAN_POINT('Ctrl Pts',(45.0807946472698,-0.381042922649615,
339.905384791082));
#29287=CARTESIAN_POINT('Ctrl Pts',(45.0730333923436,-0.244156538987243,
339.914093210447));
#29288=CARTESIAN_POINT('Ctrl Pts',(45.0652721374175,-0.107289759377202,
339.917079618029));
#29289=CARTESIAN_POINT('Ctrl Pts',(45.0574984670128,0.0297959624756219,
339.920070802889));
#29290=CARTESIAN_POINT('Ctrl Pts',(45.0497247966082,0.166861626608122,339.917321692697));
#29291=CARTESIAN_POINT('Ctrl Pts',(45.0419511262035,0.303394269079817,339.90888327219));
#29292=CARTESIAN_POINT('Ctrl Pts',(45.0345393220264,0.433571284197149,339.900837662188));
#29293=CARTESIAN_POINT('Ctrl Pts',(45.0271275178493,0.563263498892685,339.88762052584));
#29294=CARTESIAN_POINT('Ctrl Pts',(45.0197157136722,0.692035295334352,339.869319276091));
#29295=CARTESIAN_POINT('Ctrl Pts',(45.0119406348937,0.827118581110721,339.850121027575));
#29296=CARTESIAN_POINT('Ctrl Pts',(45.0041655561153,0.961615830554773,339.825267019137));
#29297=CARTESIAN_POINT('Ctrl Pts',(44.9963904773368,1.09501602186309,339.794801661629));
#29298=CARTESIAN_POINT('Ctrl Pts',(44.9886249662878,1.22825205574351,339.764373793683));
#29299=CARTESIAN_POINT('Ctrl Pts',(44.9808594552388,1.36039334018034,339.728348402073));
#29300=CARTESIAN_POINT('Ctrl Pts',(44.9730939441898,1.49093493520868,339.686821532923));
#29301=CARTESIAN_POINT('Ctrl Pts',(44.9653361326676,1.62134709786523,339.645335837785));
#29302=CARTESIAN_POINT('Ctrl Pts',(44.9575783211453,1.75016235745318,339.598359638059));
#29303=CARTESIAN_POINT('Ctrl Pts',(44.9498205096232,1.87688726920886,339.546039731589));
#29304=CARTESIAN_POINT('Ctrl Pts',(44.9420685361002,2.0035168164496,339.493759197507));
#29305=CARTESIAN_POINT('Ctrl Pts',(44.9343165625772,2.12805878710484,339.436143109465));
#29306=CARTESIAN_POINT('Ctrl Pts',(44.9265645890542,2.25003651936725,339.373387557033));
#29307=CARTESIAN_POINT('Ctrl Pts',(44.9188158984965,2.37196259398778,339.310658581615));
#29308=CARTESIAN_POINT('Ctrl Pts',(44.9110672079389,2.49132624325801,339.242794649292));
#29309=CARTESIAN_POINT('Ctrl Pts',(44.9033185173813,2.60767256698994,339.170039189968));
#29310=CARTESIAN_POINT('Ctrl Pts',(44.8955714390034,2.72399468389747,339.097298868025));
#29311=CARTESIAN_POINT('Ctrl Pts',(44.8878243606256,2.83730039276237,339.019669250516));
#29312=CARTESIAN_POINT('Ctrl Pts',(44.8800772822478,2.94716145646065,338.937438559781));
#29313=CARTESIAN_POINT('Ctrl Pts',(44.8723301389419,3.05702344090061,338.855207179874));
#29314=CARTESIAN_POINT('Ctrl Pts',(44.8645829956361,3.16344040966663,338.76837488405));
#29315=CARTESIAN_POINT('Ctrl Pts',(44.8568358523303,3.2660153835485,338.677271621314));
#29316=CARTESIAN_POINT('Ctrl Pts',(44.8490869673022,3.3686134184618,338.586147876632));
#29317=CARTESIAN_POINT('Ctrl Pts',(44.8413380822742,3.4673674475097,338.490751513853));
#29318=CARTESIAN_POINT('Ctrl Pts',(44.8335891972461,3.56191598367893,338.391450661253));
#29319=CARTESIAN_POINT('Ctrl Pts',(44.8258320874714,3.65656487464145,338.292044409701));
#29320=CARTESIAN_POINT('Ctrl Pts',(44.8180749776966,3.74699908599997,338.188725673296));
#29321=CARTESIAN_POINT('Ctrl Pts',(44.8103178679219,3.83289585922195,338.081897531531));
#29322=CARTESIAN_POINT('Ctrl Pts',(44.8025566129957,3.91883853293328,337.975012304223));
#29323=CARTESIAN_POINT('Ctrl Pts',(44.7947953580695,4.00023870530215,337.864614249265));
#29324=CARTESIAN_POINT('Ctrl Pts',(44.7870341031434,4.0768165070112,337.751136170869));
#29325=CARTESIAN_POINT('Ctrl Pts',(44.7792604327387,4.15351680824623,337.637476564529));
#29326=CARTESIAN_POINT('Ctrl Pts',(44.771486762334,4.225379118524,337.520727422123));
#29327=CARTESIAN_POINT('Ctrl Pts',(44.7637130919293,4.29216871777705,337.401347696739));
#29328=CARTESIAN_POINT('Ctrl Pts',(44.7563012877523,4.35584924511586,337.287525126294));
#29329=CARTESIAN_POINT('Ctrl Pts',(44.7488894835753,4.41491857229445,337.171311625219));
#29330=CARTESIAN_POINT('Ctrl Pts',(44.7414776793982,4.46921446891838,337.053120818001));
#29331=CARTESIAN_POINT('Ctrl Pts',(44.7337026006198,4.52617156917527,336.929137127249));
#29332=CARTESIAN_POINT('Ctrl Pts',(44.7259275218414,4.5780554823679,336.802585590731));
#29333=CARTESIAN_POINT('Ctrl Pts',(44.718152443063,4.62462701130763,336.673919970842));
#29334=CARTESIAN_POINT('Ctrl Pts',(44.710386932014,4.67114123101611,336.54541268219));
#29335=CARTESIAN_POINT('Ctrl Pts',(44.7026214209649,4.71235594191723,336.41479685046));
#29336=CARTESIAN_POINT('Ctrl Pts',(44.6948559099159,4.74807865925728,336.28254906651));
#29337=CARTESIAN_POINT('Ctrl Pts',(44.6870980983937,4.78376595741905,336.150432406623));
#29338=CARTESIAN_POINT('Ctrl Pts',(44.6793402868716,4.81397199725656,336.016687389517));
#29339=CARTESIAN_POINT('Ctrl Pts',(44.6715824753494,4.83855319293455,335.881808404158));
#29340=CARTESIAN_POINT('Ctrl Pts',(44.6638305018264,4.86311589048326,335.747030919512));
#29341=CARTESIAN_POINT('Ctrl Pts',(44.6560785283034,4.88206209940156,335.611121548152));
#29342=CARTESIAN_POINT('Ctrl Pts',(44.6483265547804,4.89529876653869,335.474587240478));
#29343=CARTESIAN_POINT('Ctrl Pts',(44.6405778642228,4.90852982793945,335.338110755165));
#29344=CARTESIAN_POINT('Ctrl Pts',(44.6328291736652,4.91605611914042,335.20101024817));
#29345=CARTESIAN_POINT('Ctrl Pts',(44.6250804831076,4.91783617294715,335.063799988657));
#29346=CARTESIAN_POINT('Ctrl Pts',(44.6173334047297,4.91961585639881,334.926618276883));
#29347=CARTESIAN_POINT('Ctrl Pts',(44.6095863263519,4.91565167542782,334.789327248607));
#29348=CARTESIAN_POINT('Ctrl Pts',(44.6018392479741,4.90595425866768,334.652442991208));
#29349=CARTESIAN_POINT('Ctrl Pts',(44.5940921046683,4.89625676063386,334.515557586587));
#29350=CARTESIAN_POINT('Ctrl Pts',(44.5863449613624,4.88082595859335,334.379079349539));
#29351=CARTESIAN_POINT('Ctrl Pts',(44.5785978180566,4.85972448547493,334.243520662691));
#29352=CARTESIAN_POINT('Ctrl Pts',(44.5708489330285,4.83861826829729,334.107931499372));
#29353=CARTESIAN_POINT('Ctrl Pts',(44.5631000480004,4.81183890326738,333.973262683779));
#29354=CARTESIAN_POINT('Ctrl Pts',(44.5553511629723,4.77950033593997,333.840017413385));
#29355=CARTESIAN_POINT('Ctrl Pts',(44.5475940531976,4.74712744412307,333.706630715085));
#29356=CARTESIAN_POINT('Ctrl Pts',(44.5398369434229,4.70918365535144,333.574670960727));
#29357=CARTESIAN_POINT('Ctrl Pts',(44.5320798336481,4.66583326460921,333.444627694291));
#29358=CARTESIAN_POINT('Ctrl Pts',(44.524318578722,4.62245970880426,333.314514936891));
#29359=CARTESIAN_POINT('Ctrl Pts',(44.5165573237958,4.57367393316091,333.186321073173));
#29360=CARTESIAN_POINT('Ctrl Pts',(44.5087960688696,4.51968843862668,333.060515666409));
#29361=CARTESIAN_POINT('Ctrl Pts',(44.5010223984649,4.46561658489511,332.934509011994));
#29362=CARTESIAN_POINT('Ctrl Pts',(44.4932487280603,4.40632855986221,332.810898802147));
#29363=CARTESIAN_POINT('Ctrl Pts',(44.4854750576557,4.34208328647498,332.690130783829));
#29364=CARTESIAN_POINT('Ctrl Pts',(44.4780632534785,4.28082864602001,332.574984545818));
#29365=CARTESIAN_POINT('Ctrl Pts',(44.4706514493014,4.21506803599211,332.462422094642));
#29366=CARTESIAN_POINT('Ctrl Pts',(44.4632396451243,4.14506148987295,332.352803689245));
#29367=CARTESIAN_POINT('Ctrl Pts',(44.4554645663458,4.07162371439012,332.237812559264));
#29368=CARTESIAN_POINT('Ctrl Pts',(44.4476894875674,3.99328118999983,332.12569797183));
#29369=CARTESIAN_POINT('Ctrl Pts',(44.4399144087889,3.91028605185769,332.016906629831));
#29370=CARTESIAN_POINT('Ctrl Pts',(44.4321488977399,3.82739304451675,331.908249162504));
#29371=CARTESIAN_POINT('Ctrl Pts',(44.4243833866909,3.73985905001655,331.802907111546));
#29372=CARTESIAN_POINT('Ctrl Pts',(44.4166178756419,3.64798067923199,331.701300252152));
#29373=CARTESIAN_POINT('Ctrl Pts',(44.4088600641197,3.55619340611961,331.599794136256));
#29374=CARTESIAN_POINT('Ctrl Pts',(44.4011022525975,3.46007058928822,331.502016129895));
#29375=CARTESIAN_POINT('Ctrl Pts',(44.3933444410753,3.35995026843267,331.4083545197));
#29376=CARTESIAN_POINT('Ctrl Pts',(44.3855924675523,3.25990529129357,331.314763392837));
#29377=CARTESIAN_POINT('Ctrl Pts',(44.3778404940293,3.15586908219602,331.225282762237));
#29378=CARTESIAN_POINT('Ctrl Pts',(44.3700885205063,3.04821759014883,331.14026521823));
#29379=CARTESIAN_POINT('Ctrl Pts',(44.3623398299486,2.94061168857243,331.055283679203));
#29380=CARTESIAN_POINT('Ctrl Pts',(44.354591139391,2.82939385535681,330.974761709206));
#29381=CARTESIAN_POINT('Ctrl Pts',(44.3468424488334,2.71497411013338,330.899012479438));
#29382=CARTESIAN_POINT('Ctrl Pts',(44.3390953704555,2.60057817089359,330.82327900993));
#29383=CARTESIAN_POINT('Ctrl Pts',(44.3313482920777,2.48298197045246,330.752316521123));
#29384=CARTESIAN_POINT('Ctrl Pts',(44.3236012136999,2.36262524946094,330.686395359666));
#29385=CARTESIAN_POINT('Ctrl Pts',(44.315854070394,2.24226751976384,330.620473645726));
#29386=CARTESIAN_POINT('Ctrl Pts',(44.3081069270882,2.11914956619075,330.559593531177));
#29387=CARTESIAN_POINT('Ctrl Pts',(44.3003597837824,1.99373615649516,330.503979626294));
#29388=CARTESIAN_POINT('Ctrl Pts',(44.2926108987543,1.86829455120333,330.448353218223));
#29389=CARTESIAN_POINT('Ctrl Pts',(44.2848620137263,1.7405568201209,330.397995534178));
#29390=CARTESIAN_POINT('Ctrl Pts',(44.2771131286982,1.6110077752169,330.353083063935));
#29391=CARTESIAN_POINT('Ctrl Pts',(44.2693560189235,1.48132122561779,330.308122923132));
#29392=CARTESIAN_POINT('Ctrl Pts',(44.2615989091487,1.3498198916223,330.268619669673));
#29393=CARTESIAN_POINT('Ctrl Pts',(44.253841799374,1.21700435064926,330.234700064739));
#29394=CARTESIAN_POINT('Ctrl Pts',(44.2460805444478,1.08411783729764,330.200762334252));
#29395=CARTESIAN_POINT('Ctrl Pts',(44.2383192895217,0.949916099873101,330.172414278369));
#29396=CARTESIAN_POINT('Ctrl Pts',(44.2305580345955,0.814909000605078,330.14973130814));
#29397=CARTESIAN_POINT('Ctrl Pts',(44.2227843641909,0.679685933976937,330.127012052552));
#29398=CARTESIAN_POINT('Ctrl Pts',(44.2150106937862,0.543655319116055,330.109976040355));
#29399=CARTESIAN_POINT('Ctrl Pts',(44.2072370233815,0.407332112217123,330.098646756981));
#29400=CARTESIAN_POINT('Ctrl Pts',(44.1998252192045,0.277354783397359,330.087844854473));
#29401=CARTESIAN_POINT('Ctrl Pts',(44.1924134150274,0.14711177736114,330.082230353223));
#29402=CARTESIAN_POINT('Ctrl Pts',(44.1850016108504,0.0170467625781974,
330.081779542316));
#29403=CARTESIAN_POINT('Ctrl Pts',(44.1772265320719,-0.119393126023619,
330.081306635823));
#29404=CARTESIAN_POINT('Ctrl Pts',(44.1694514532935,-0.256068309697689,
330.086514899553));
#29405=CARTESIAN_POINT('Ctrl Pts',(44.161676374515,-0.392466701654937,330.097434044238));
#29406=CARTESIAN_POINT('Ctrl Pts',(44.153910863466,-0.52869724670715,330.108339752222));
#29407=CARTESIAN_POINT('Ctrl Pts',(44.146145352417,-0.664651291855306,330.124942327354));
#29408=CARTESIAN_POINT('Ctrl Pts',(44.138379841368,-0.799815326017855,330.147219507667));
#29409=CARTESIAN_POINT('Ctrl Pts',(44.1306220298458,-0.934845344647104,
330.169474600092));
#29410=CARTESIAN_POINT('Ctrl Pts',(44.1228642183236,-1.06908652791168,330.197393037713));
#29411=CARTESIAN_POINT('Ctrl Pts',(44.1151064068014,-1.20202942462513,330.230900679915));
#29412=CARTESIAN_POINT('Ctrl Pts',(44.1073544332784,-1.33487227759277,330.264383106554));
#29413=CARTESIAN_POINT('Ctrl Pts',(44.0996024597554,-1.4664184111891,330.303446270684));
#29414=CARTESIAN_POINT('Ctrl Pts',(44.0918504862323,-1.59616787710212,330.347964835622));
#29415=CARTESIAN_POINT('Ctrl Pts',(44.0841017956747,-1.72586239403947,330.392464546922));
#29416=CARTESIAN_POINT('Ctrl Pts',(44.0763531051172,-1.85376138770215,330.442414937286));
#29417=CARTESIAN_POINT('Ctrl Pts',(44.0686044145595,-1.97937962059679,330.497640687366));
#29418=CARTESIAN_POINT('Ctrl Pts',(44.0608573361817,-2.10497171756873,330.552854947266));
#29419=CARTESIAN_POINT('Ctrl Pts',(44.0531102578039,-2.22828364005197,330.613342226502));
#29420=CARTESIAN_POINT('Ctrl Pts',(44.045363179426,-2.34885007888299,330.678879037862));
#29421=CARTESIAN_POINT('Ctrl Pts',(44.0376160361202,-2.46941752817672,330.744416398483));
#29422=CARTESIAN_POINT('Ctrl Pts',(44.0298688928144,-2.58723910450557,330.815003188966));
#29423=CARTESIAN_POINT('Ctrl Pts',(44.0221217495086,-2.70187441579872,330.890370125698));
#29424=CARTESIAN_POINT('Ctrl Pts',(44.0143728644805,-2.8165354995441,330.965754006519));
#29425=CARTESIAN_POINT('Ctrl Pts',(44.0066239794524,-2.92800856627114,331.045919957391));
#29426=CARTESIAN_POINT('Ctrl Pts',(43.9988750944243,-3.03588284238472,331.130555798333));
#29427=CARTESIAN_POINT('Ctrl Pts',(43.9911179846496,-3.14387161736908,331.215281472631));
#29428=CARTESIAN_POINT('Ctrl Pts',(43.9833608748749,-3.24825366333711,331.304486272703));
#29429=CARTESIAN_POINT('Ctrl Pts',(43.9756037651002,-3.34865149294404,331.397817850066));
#29430=CARTESIAN_POINT('Ctrl Pts',(43.967842510174,-3.44910297194108,331.49119930084));
#29431=CARTESIAN_POINT('Ctrl Pts',(43.9600812552479,-3.54556571752651,331.588711645259));
#29432=CARTESIAN_POINT('Ctrl Pts',(43.9523200003217,-3.63770039923142,331.689966938544));
#29433=CARTESIAN_POINT('Ctrl Pts',(43.944546329917,-3.72998246640044,331.791384207299));
#29434=CARTESIAN_POINT('Ctrl Pts',(43.9367726595124,-3.81792238363982,331.896556089696));
#29435=CARTESIAN_POINT('Ctrl Pts',(43.9289989891077,-3.90122172920631,332.005062257397));
#29436=CARTESIAN_POINT('Ctrl Pts',(43.9215871849306,-3.98064347019634,332.108517436887));
#29437=CARTESIAN_POINT('Ctrl Pts',(43.9141753807535,-4.05584678798625,332.21500323049));
#29438=CARTESIAN_POINT('Ctrl Pts',(43.9067635765764,-4.12661152712434,332.324133716587));
#29439=CARTESIAN_POINT('Ctrl Pts',(43.89881824557,-4.20247015244647,332.441119785595));
#29440=CARTESIAN_POINT('Ctrl Pts',(43.8908729145636,-4.27345962110023,332.561502301101));
#29441=CARTESIAN_POINT('Ctrl Pts',(43.8829275835573,-4.33926899970426,332.684848253201));
#29442=CARTESIAN_POINT('Ctrl Pts',(43.8749932764454,-4.40498706988476,332.808023066709));
#29443=CARTESIAN_POINT('Ctrl Pts',(43.8670589693336,-4.46553918750092,332.934152809086));
#29444=CARTESIAN_POINT('Ctrl Pts',(43.8591246622217,-4.5206574553238,333.062775378505));
#29445=CARTESIAN_POINT('Ctrl Pts',(43.8511999370428,-4.57570915910553,333.191242615793));
#29446=CARTESIAN_POINT('Ctrl Pts',(43.8432752118639,-4.62533993597997,333.322196349463));
#29447=CARTESIAN_POINT('Ctrl Pts',(43.8353504866849,-4.66932768418344,333.455149832437));
#29448=CARTESIAN_POINT('Ctrl Pts',(43.8274359625603,-4.71325880942557,333.58793217185));
#29449=CARTESIAN_POINT('Ctrl Pts',(43.8195214384357,-4.7515612687418,333.722708782192));
#29450=CARTESIAN_POINT('Ctrl Pts',(43.811606914311,-4.78406117279454,333.858973375657));
#29451=CARTESIAN_POINT('Ctrl Pts',(43.8036983779828,-4.81653648878549,333.995134877056));
#29452=CARTESIAN_POINT('Ctrl Pts',(43.7957898416545,-4.84321790503991,334.13278176346));
#29453=CARTESIAN_POINT('Ctrl Pts',(43.7878813053263,-4.86398132358368,334.271392597945));
#29454=CARTESIAN_POINT('Ctrl Pts',(43.7799779889375,-4.88473103746923,334.409911943925));
#29455=CARTESIAN_POINT('Ctrl Pts',(43.7720746725487,-4.89957048181482,334.549393607077));
#29456=CARTESIAN_POINT('Ctrl Pts',(43.7641713561599,-4.90842667497265,334.689306197492));
#29457=CARTESIAN_POINT('Ctrl Pts',(43.7582929869366,-4.91501377976932,334.793371102018));
#29458=CARTESIAN_POINT('Ctrl Pts',(43.7524146177133,-4.9182919013256,334.897674145527));
#29459=CARTESIAN_POINT('Ctrl Pts',(43.7465362484901,-4.91824959557215,335.001994531113));
#29460=CARTESIAN_POINT('',(47.246536248526,-4.91824999896793,335.000100756667));
#29461=CARTESIAN_POINT('Ctrl Pts',(47.2465362484901,-4.91824999896792,335.000100757296));
#29462=CARTESIAN_POINT('Ctrl Pts',(47.2462308282813,-4.91824988916758,335.005460423983));
#29463=CARTESIAN_POINT('Ctrl Pts',(47.2459254080725,-4.9182410183197,335.010820080069));
#29464=CARTESIAN_POINT('Ctrl Pts',(47.2456199878637,-4.91822338650565,335.016179707317));
#29465=CARTESIAN_POINT('Ctrl Pts',(47.2378449090853,-4.91777453361609,335.152619677169));
#29466=CARTESIAN_POINT('Ctrl Pts',(47.2300698303068,-4.91164305056294,335.289256556375));
#29467=CARTESIAN_POINT('Ctrl Pts',(47.2222947515284,-4.89980268680175,335.425578069113));
#29468=CARTESIAN_POINT('Ctrl Pts',(47.2145292404793,-4.88797689336197,335.561731829552));
#29469=CARTESIAN_POINT('Ctrl Pts',(47.2067637294303,-4.87045623072988,335.697570610002));
#29470=CARTESIAN_POINT('Ctrl Pts',(47.1989982183813,-4.84726642949793,335.832581061496));
#29471=CARTESIAN_POINT('Ctrl Pts',(47.1912404068591,-4.82409962102142,335.967457649735));
#29472=CARTESIAN_POINT('Ctrl Pts',(47.1834825953368,-4.79527492573058,336.101507160681));
#29473=CARTESIAN_POINT('Ctrl Pts',(47.1757247838146,-4.76086992425483,336.234220655647));
#29474=CARTESIAN_POINT('Ctrl Pts',(47.1679728102916,-4.7264908136338,336.366834279499));
#29475=CARTESIAN_POINT('Ctrl Pts',(47.1602208367686,-4.68653985313726,336.498113511716));
#29476=CARTESIAN_POINT('Ctrl Pts',(47.1524688632456,-4.64114575409418,336.627559262133));
#29477=CARTESIAN_POINT('Ctrl Pts',(47.1447201726879,-4.59577087947888,336.756950192198));
#29478=CARTESIAN_POINT('Ctrl Pts',(47.1369714821304,-4.54495758022238,336.884508816744));
#29479=CARTESIAN_POINT('Ctrl Pts',(47.1292227915727,-4.4888844497976,337.009751093759));
#29480=CARTESIAN_POINT('Ctrl Pts',(47.1214757131949,-4.43282298585593,337.134967313072));
#29481=CARTESIAN_POINT('Ctrl Pts',(47.113728634817,-4.37150402711232,337.25786778693));
#29482=CARTESIAN_POINT('Ctrl Pts',(47.1059815564392,-4.30515419917185,337.377988726603));
#29483=CARTESIAN_POINT('Ctrl Pts',(47.0982344131333,-4.23880381515596,337.498110673006));
#29484=CARTESIAN_POINT('Ctrl Pts',(47.0904872698275,-4.16742266683379,337.615452696611));
#29485=CARTESIAN_POINT('Ctrl Pts',(47.0827401265217,-4.09128300683433,337.729576234599));
#29486=CARTESIAN_POINT('Ctrl Pts',(47.0749912414936,-4.01512622902287,337.843725429982));
#29487=CARTESIAN_POINT('Ctrl Pts',(47.0672423564654,-3.93420902761155,337.954654374809));
#29488=CARTESIAN_POINT('Ctrl Pts',(47.0594934714373,-3.84884635052599,338.061954413858));
#29489=CARTESIAN_POINT('Ctrl Pts',(47.0517363616626,-3.7633930686129,338.169368342277));
#29490=CARTESIAN_POINT('Ctrl Pts',(47.0439792518879,-3.67348512916239,338.273145364301));
#29491=CARTESIAN_POINT('Ctrl Pts',(47.0362221421131,-3.57947742281258,338.372910381566));
#29492=CARTESIAN_POINT('Ctrl Pts',(47.0284608871869,-3.48541948175034,338.472728710066));
#29493=CARTESIAN_POINT('Ctrl Pts',(47.0206996322608,-3.38725768804384,338.56853048905));
#29494=CARTESIAN_POINT('Ctrl Pts',(47.0129383773346,-3.28538227003903,338.659979016636));
#29495=CARTESIAN_POINT('Ctrl Pts',(47.0051647069299,-3.18334388456646,338.751573832063));
#29496=CARTESIAN_POINT('Ctrl Pts',(46.9973910365252,-3.07758030544742,338.83880123156));
#29497=CARTESIAN_POINT('Ctrl Pts',(46.9896173661205,-2.96851386747844,338.921365639811));
#29498=CARTESIAN_POINT('Ctrl Pts',(46.9822055619436,-2.86452449843929,339.000086654992));
#29499=CARTESIAN_POINT('Ctrl Pts',(46.9747937577667,-2.7575330828981,339.074568869282));
#29500=CARTESIAN_POINT('Ctrl Pts',(46.9673819535897,-2.64792702097345,339.144594739429));
#29501=CARTESIAN_POINT('Ctrl Pts',(46.9596068748113,-2.53294883945196,339.218052786069));
#29502=CARTESIAN_POINT('Ctrl Pts',(46.9518317960329,-2.41472987540388,339.28683874672));
#29503=CARTESIAN_POINT('Ctrl Pts',(46.9440567172544,-2.29368670681961,339.350653324899));
#29504=CARTESIAN_POINT('Ctrl Pts',(46.9362912062054,-2.17279248956019,339.414389375178));
#29505=CARTESIAN_POINT('Ctrl Pts',(46.9285256951564,-2.04908132520099,339.473166034713));
#29506=CARTESIAN_POINT('Ctrl Pts',(46.9207601841074,-1.92299882414081,339.526727138326));
#29507=CARTESIAN_POINT('Ctrl Pts',(46.9130023725852,-1.79704133424759,339.580235135948));
#29508=CARTESIAN_POINT('Ctrl Pts',(46.905244561063,-1.66871754408978,339.628537716863));
#29509=CARTESIAN_POINT('Ctrl Pts',(46.8974867495408,-1.53849741439805,339.671424704348));
#29510=CARTESIAN_POINT('Ctrl Pts',(46.8897347760178,-1.40837527948344,339.714279418015));
#29511=CARTESIAN_POINT('Ctrl Pts',(46.8819828024948,-1.27636001528255,339.75172652837));
#29512=CARTESIAN_POINT('Ctrl Pts',(46.8742308289718,-1.142940970448,339.78360418519));
#29513=CARTESIAN_POINT('Ctrl Pts',(46.8664821384142,-1.00957842865815,339.815468341804));
#29514=CARTESIAN_POINT('Ctrl Pts',(46.8587334478566,-0.874813668039296,
339.84176764546));
#29515=CARTESIAN_POINT('Ctrl Pts',(46.8509847572989,-0.739150377022791,
339.862390336311));
#29516=CARTESIAN_POINT('Ctrl Pts',(46.8432376789211,-0.60351531188697,339.883008736439));
#29517=CARTESIAN_POINT('Ctrl Pts',(46.8354906005432,-0.46698247439608,339.897952814281));
#29518=CARTESIAN_POINT('Ctrl Pts',(46.8277435221654,-0.330064514506286,
339.90716216145));
#29519=CARTESIAN_POINT('Ctrl Pts',(46.8199963788596,-0.193145407112298,
339.916371585802));
#29520=CARTESIAN_POINT('Ctrl Pts',(46.8122492355538,-0.0558415608746182,
339.919846157384));
#29521=CARTESIAN_POINT('Ctrl Pts',(46.804502092248,0.0813308958569487,339.917577487735));
#29522=CARTESIAN_POINT('Ctrl Pts',(46.7967532072199,0.218534191869136,339.915308308041));
#29523=CARTESIAN_POINT('Ctrl Pts',(46.7890043221918,0.355605648851132,339.907293324229));
#29524=CARTESIAN_POINT('Ctrl Pts',(46.7812554371637,0.492031183513202,339.893576235939));
#29525=CARTESIAN_POINT('Ctrl Pts',(46.773498327389,0.628601521647209,339.87984458819));
#29526=CARTESIAN_POINT('Ctrl Pts',(46.7657412176142,0.764524178406057,339.860398785147));
#29527=CARTESIAN_POINT('Ctrl Pts',(46.7579841078395,0.899291673883825,339.835334274668));
#29528=CARTESIAN_POINT('Ctrl Pts',(46.7502228529133,1.03413118480224,339.810256370517));
#29529=CARTESIAN_POINT('Ctrl Pts',(46.7424615979872,1.16781392368806,339.779553863713));
#29530=CARTESIAN_POINT('Ctrl Pts',(46.734700343061,1.29984557579606,339.743372696888));
#29531=CARTESIAN_POINT('Ctrl Pts',(46.7269266726564,1.43208843551832,339.707133651988));
#29532=CARTESIAN_POINT('Ctrl Pts',(46.7191530022517,1.56267455804415,339.665398552915));
#29533=CARTESIAN_POINT('Ctrl Pts',(46.711379331847,1.69112683819248,339.618362597246));
#29534=CARTESIAN_POINT('Ctrl Pts',(46.7039675276699,1.81359963379623,339.57351617663));
#29535=CARTESIAN_POINT('Ctrl Pts',(46.6965557234929,1.93413251091924,339.52385141268));
#29536=CARTESIAN_POINT('Ctrl Pts',(46.6891439193158,2.05233288836629,339.469576353283));
#29537=CARTESIAN_POINT('Ctrl Pts',(46.6813688405373,2.17632661841252,339.412641111549));
#29538=CARTESIAN_POINT('Ctrl Pts',(46.6735937617589,2.29814526505762,339.350452292836));
#29539=CARTESIAN_POINT('Ctrl Pts',(46.6658186829804,2.41731170924942,339.283198239963));
#29540=CARTESIAN_POINT('Ctrl Pts',(46.6580531719314,2.53633151154506,339.216026947484));
#29541=CARTESIAN_POINT('Ctrl Pts',(46.6502876608825,2.65270526807261,339.143803013191));
#29542=CARTESIAN_POINT('Ctrl Pts',(46.6425221498335,2.76597641871267,339.066762534698));
#29543=CARTESIAN_POINT('Ctrl Pts',(46.6347643383113,2.87913526067709,338.989798442064));
#29544=CARTESIAN_POINT('Ctrl Pts',(46.6270065267891,2.98919729753012,338.908027527387));
#29545=CARTESIAN_POINT('Ctrl Pts',(46.619248715267,3.09573146446576,338.821731251987));
#29546=CARTESIAN_POINT('Ctrl Pts',(46.611496741744,3.20218546106231,338.735499917272));
#29547=CARTESIAN_POINT('Ctrl Pts',(46.603744768221,3.30511656955243,338.644750245312));
#29548=CARTESIAN_POINT('Ctrl Pts',(46.595992794698,3.40412387199562,338.549806153385));
#29549=CARTESIAN_POINT('Ctrl Pts',(46.5882441041404,3.50308924478751,338.454902270338));
#29550=CARTESIAN_POINT('Ctrl Pts',(46.5804954135828,3.59813383507359,338.355807770315));
#29551=CARTESIAN_POINT('Ctrl Pts',(46.5727467230251,3.68889108690309,338.252885735999));
#29552=CARTESIAN_POINT('Ctrl Pts',(46.5649996446473,3.77962945592833,338.149985115472));
#29553=CARTESIAN_POINT('Ctrl Pts',(46.5572525662695,3.86608200242266,338.043258837638));
#29554=CARTESIAN_POINT('Ctrl Pts',(46.5495054878917,3.94792050337689,337.933105310335));
#29555=CARTESIAN_POINT('Ctrl Pts',(46.5417583445859,4.02975969021658,337.82295085984));
#29556=CARTESIAN_POINT('Ctrl Pts',(46.5340112012801,4.1069845212793,337.709369416344));
#29557=CARTESIAN_POINT('Ctrl Pts',(46.5262640579743,4.17930863586297,337.592790463709));
#29558=CARTESIAN_POINT('Ctrl Pts',(46.5185151729462,4.251649010443,337.476185301651));
#29559=CARTESIAN_POINT('Ctrl Pts',(46.5107662879181,4.31908627009488,337.356581621544));
#29560=CARTESIAN_POINT('Ctrl Pts',(46.5030174028901,4.38137896281191,337.234435375375));
#29561=CARTESIAN_POINT('Ctrl Pts',(46.4952602931154,4.44373777363664,337.11215948192));
#29562=CARTESIAN_POINT('Ctrl Pts',(46.4875031833407,4.5009409318119,336.987335980242));
#29563=CARTESIAN_POINT('Ctrl Pts',(46.479746073566,4.55279407498322,336.860443273335));
#29564=CARTESIAN_POINT('Ctrl Pts',(46.4719848186398,4.60467492681631,336.733482759023));
#29565=CARTESIAN_POINT('Ctrl Pts',(46.4642235637137,4.65119993456036,336.604451203757));
#29566=CARTESIAN_POINT('Ctrl Pts',(46.4564623087875,4.6922243224165,336.473843265284));
#29567=CARTESIAN_POINT('Ctrl Pts',(46.4486886383829,4.7333143359234,336.343026396675));
#29568=CARTESIAN_POINT('Ctrl Pts',(46.4409149679782,4.76888604466275,336.210628483442));
#29569=CARTESIAN_POINT('Ctrl Pts',(46.4331412975735,4.79884540545156,336.077156366122));
#29570=CARTESIAN_POINT('Ctrl Pts',(46.4257294933963,4.82741015078846,335.949897407971));
#29571=CARTESIAN_POINT('Ctrl Pts',(46.4183176892191,4.85087324721813,335.821662286603));
#29572=CARTESIAN_POINT('Ctrl Pts',(46.4109058850419,4.8691971984371,335.692893718569));
#29573=CARTESIAN_POINT('Ctrl Pts',(46.4031308062634,4.88841926108922,335.557813819436));
#29574=CARTESIAN_POINT('Ctrl Pts',(46.395355727485,4.90204641634547,335.421719982386));
#29575=CARTESIAN_POINT('Ctrl Pts',(46.3875806487065,4.90997884920386,335.285115350114));
#29576=CARTESIAN_POINT('Ctrl Pts',(46.3798151376575,4.91790152069862,335.148678818539));
#29577=CARTESIAN_POINT('Ctrl Pts',(46.3720496266085,4.92014339070318,335.011733128895));
#29578=CARTESIAN_POINT('Ctrl Pts',(46.3642841155595,4.91665592786032,334.874789978293));
#29579=CARTESIAN_POINT('Ctrl Pts',(46.3565263040373,4.91317192284702,334.737982607223));
#29580=CARTESIAN_POINT('Ctrl Pts',(46.348768492515,4.90396989968825,334.601178158416));
#29581=CARTESIAN_POINT('Ctrl Pts',(46.3410106809928,4.88905327131267,334.464891438335));
#29582=CARTESIAN_POINT('Ctrl Pts',(46.3332587074698,4.87414786817297,334.328707278333));
#29583=CARTESIAN_POINT('Ctrl Pts',(46.3255067339468,4.85353646195163,334.193040458551));
#29584=CARTESIAN_POINT('Ctrl Pts',(46.3177547604238,4.8272744818967,334.058403409666));
#29585=CARTESIAN_POINT('Ctrl Pts',(46.3100060698661,4.80102362380593,333.923823379651));
#29586=CARTESIAN_POINT('Ctrl Pts',(46.3022573793085,4.76912702610943,333.790272635988));
#29587=CARTESIAN_POINT('Ctrl Pts',(46.2945086887509,4.73169164832267,333.65825590827));
#29588=CARTESIAN_POINT('Ctrl Pts',(46.286761610373,4.69426405927893,333.526266647734));
#29589=CARTESIAN_POINT('Ctrl Pts',(46.2790145319952,4.65130008889624,333.395811144114));
#29590=CARTESIAN_POINT('Ctrl Pts',(46.2712674536173,4.60295714652336,333.267381008482));
#29591=CARTESIAN_POINT('Ctrl Pts',(46.2635203103115,4.55461379899007,333.138949796482));
#29592=CARTESIAN_POINT('Ctrl Pts',(46.2557731670057,4.50089152724785,333.012544352144));
#29593=CARTESIAN_POINT('Ctrl Pts',(46.2480260236999,4.441996527232,332.888637900653));
#29594=CARTESIAN_POINT('Ctrl Pts',(46.2402771386717,4.38308828636985,332.764703592362));
#29595=CARTESIAN_POINT('Ctrl Pts',(46.2325282536437,4.31900517088127,332.643269747846));
#29596=CARTESIAN_POINT('Ctrl Pts',(46.2247793686155,4.24999993698532,332.524786151032));
#29597=CARTESIAN_POINT('Ctrl Pts',(46.2170222588408,4.18092146022106,332.406176794504));
#29598=CARTESIAN_POINT('Ctrl Pts',(46.2092651490661,4.10691062587209,332.290524279289));
#29599=CARTESIAN_POINT('Ctrl Pts',(46.2015080392913,4.02826455259932,332.178250940149));
#29600=CARTESIAN_POINT('Ctrl Pts',(46.1937467843651,3.94957645337966,332.065917605726));
#29601=CARTESIAN_POINT('Ctrl Pts',(46.185985529439,3.86624841708287,331.956967355762));
#29602=CARTESIAN_POINT('Ctrl Pts',(46.1782242745128,3.77861806547016,331.851789623008));
#29603=CARTESIAN_POINT('Ctrl Pts',(46.1704506041081,3.69084753385355,331.746443640158));
#29604=CARTESIAN_POINT('Ctrl Pts',(46.1626769337034,3.59876119673338,331.644882523549));
#29605=CARTESIAN_POINT('Ctrl Pts',(46.1549032632988,3.50273437496572,331.547459636596));
#29606=CARTESIAN_POINT('Ctrl Pts',(46.1474914591218,3.411177624856,331.454571808471));
#29607=CARTESIAN_POINT('Ctrl Pts',(46.1400796549449,3.31603920331488,331.365445807822));
#29608=CARTESIAN_POINT('Ctrl Pts',(46.1326678507679,3.21767110873487,331.280352745419));
#29609=CARTESIAN_POINT('Ctrl Pts',(46.1248927719895,3.11448170081422,331.191089018547));
#29610=CARTESIAN_POINT('Ctrl Pts',(46.1171176932111,3.00741192543951,331.105981468679));
#29611=CARTESIAN_POINT('Ctrl Pts',(46.1093426144327,2.89683087041296,331.025386311763));
#29612=CARTESIAN_POINT('Ctrl Pts',(46.1015771033837,2.78638589241456,330.944890332318));
#29613=CARTESIAN_POINT('Ctrl Pts',(46.0938115923347,2.67243854488297,330.868895925395));
#29614=CARTESIAN_POINT('Ctrl Pts',(46.0860460812857,2.55539286173332,330.797720810714));
#29615=CARTESIAN_POINT('Ctrl Pts',(46.0782882697635,2.4384632297192,330.726616266367));
#29616=CARTESIAN_POINT('Ctrl Pts',(46.0705304582413,2.31844170737988,330.660321706871));
#29617=CARTESIAN_POINT('Ctrl Pts',(46.0627726467191,2.19576305338438,330.599112853538));
#29618=CARTESIAN_POINT('Ctrl Pts',(46.0550206731961,2.07317671896638,330.537950061809));
#29619=CARTESIAN_POINT('Ctrl Pts',(46.0472686996731,1.94793758129912,330.481865532281));
#29620=CARTESIAN_POINT('Ctrl Pts',(46.0395167261501,1.82050655021642,330.43108995896));
#29621=CARTESIAN_POINT('Ctrl Pts',(46.0317680355924,1.69312948625113,330.380335889124));
#29622=CARTESIAN_POINT('Ctrl Pts',(46.0240193450349,1.56356273748543,330.334886448075));
#29623=CARTESIAN_POINT('Ctrl Pts',(46.0162706544773,1.4322886237324,330.294924829418));
#29624=CARTESIAN_POINT('Ctrl Pts',(46.0085235760994,1.30104182265517,330.25497152511));
#29625=CARTESIAN_POINT('Ctrl Pts',(46.0007764977216,1.16808873686888,330.220503885856));
#29626=CARTESIAN_POINT('Ctrl Pts',(45.9930294193438,1.03392795584425,330.191655581739));
#29627=CARTESIAN_POINT('Ctrl Pts',(45.985282276038,0.899766050423068,330.162807035845));
#29628=CARTESIAN_POINT('Ctrl Pts',(45.9775351327322,0.764396811714784,330.139578001193));
#29629=CARTESIAN_POINT('Ctrl Pts',(45.9697879894264,0.628329769325667,330.122051172524));
#29630=CARTESIAN_POINT('Ctrl Pts',(45.9620391043983,0.492232136176728,330.104520403451));
#29631=CARTESIAN_POINT('Ctrl Pts',(45.9542902193702,0.355436774766759,330.092694441278));
#29632=CARTESIAN_POINT('Ctrl Pts',(45.9465413343421,0.218458698889019,330.0866041418));
#29633=CARTESIAN_POINT('Ctrl Pts',(45.9387842245674,0.0813352330662,330.080507378014));
#29634=CARTESIAN_POINT('Ctrl Pts',(45.9310271147927,-0.0559709435225165,
330.080158455448));
#29635=CARTESIAN_POINT('Ctrl Pts',(45.923270005018,-0.192943892610512,330.085536070251));
#29636=CARTESIAN_POINT('Ctrl Pts',(45.9155087500918,-0.329990035662955,
330.09091655868));
#29637=CARTESIAN_POINT('Ctrl Pts',(45.9077474951657,-0.466702207010266,
330.102029650308));
#29638=CARTESIAN_POINT('Ctrl Pts',(45.8999862402395,-0.602570217838123,
330.1188021762));
#29639=CARTESIAN_POINT('Ctrl Pts',(45.8922125698349,-0.73865557320393,330.135601532666));
#29640=CARTESIAN_POINT('Ctrl Pts',(45.8844388994303,-0.873893683799842,
330.158078350353));
#29641=CARTESIAN_POINT('Ctrl Pts',(45.8766652290256,-1.00778429114064,330.186108239165));
#29642=CARTESIAN_POINT('Ctrl Pts',(45.8692534248484,-1.13544225849978,330.21283332991));
#29643=CARTESIAN_POINT('Ctrl Pts',(45.8618416206712,-1.26187507280759,330.244606065274));
#29644=CARTESIAN_POINT('Ctrl Pts',(45.854429816494,-1.38666426470488,330.281277155894));
#29645=CARTESIAN_POINT('Ctrl Pts',(45.8466547377155,-1.51756974662326,330.319745605902));
#29646=CARTESIAN_POINT('Ctrl Pts',(45.8388796589371,-1.64708010011546,330.363726285544));
#29647=CARTESIAN_POINT('Ctrl Pts',(45.8311045801586,-1.7746960410034,330.413101589903));
#29648=CARTESIAN_POINT('Ctrl Pts',(45.8233390691096,-1.90215494235157,330.462416134807));
#29649=CARTESIAN_POINT('Ctrl Pts',(45.8155735580605,-2.02772370845022,330.517111956162));
#29650=CARTESIAN_POINT('Ctrl Pts',(45.8078080470115,-2.15091651607223,330.577021229602));
#29651=CARTESIAN_POINT('Ctrl Pts',(45.8000502354893,-2.27398717766699,330.636871102824));
#29652=CARTESIAN_POINT('Ctrl Pts',(45.7922924239671,-2.39468621965149,330.701923971382));
#29653=CARTESIAN_POINT('Ctrl Pts',(45.7845346124448,-2.51254650922983,330.771963446059));
#29654=CARTESIAN_POINT('Ctrl Pts',(45.7767826389218,-2.63031810520262,330.841950213812));
#29655=CARTESIAN_POINT('Ctrl Pts',(45.7690306653988,-2.74525486620574,330.916915919479));
#29656=CARTESIAN_POINT('Ctrl Pts',(45.7612786918758,-2.85691337197112,330.996597815913));
#29657=CARTESIAN_POINT('Ctrl Pts',(45.7535300013181,-2.96852459029293,331.076245967016));
#29658=CARTESIAN_POINT('Ctrl Pts',(45.7457813107605,-3.0768599971882,331.160606109799));
#29659=CARTESIAN_POINT('Ctrl Pts',(45.7380326202029,-3.18150453031966,331.249371787813));
#29660=CARTESIAN_POINT('Ctrl Pts',(45.730285541825,-3.28612729128206,331.338118997385));
#29661=CARTESIAN_POINT('Ctrl Pts',(45.7225384634472,-3.38706040803083,331.431269666301));
#29662=CARTESIAN_POINT('Ctrl Pts',(45.7147913850693,-3.48392165917142,331.528476856586));
#29663=CARTESIAN_POINT('Ctrl Pts',(45.7070442417635,-3.58078372210252,331.625684861562));
#29664=CARTESIAN_POINT('Ctrl Pts',(45.6992970984577,-3.67357357546152,331.726949178837));
#29665=CARTESIAN_POINT('Ctrl Pts',(45.6915499551519,-3.76194594377021,331.831886084963));
#29666=CARTESIAN_POINT('Ctrl Pts',(45.6838010701237,-3.85033818006337,331.936846583134));
#29667=CARTESIAN_POINT('Ctrl Pts',(45.6760521850956,-3.93431070332546,332.04548101424));
#29668=CARTESIAN_POINT('Ctrl Pts',(45.6683033000675,-4.01355886274549,332.157372990036));
#29669=CARTESIAN_POINT('Ctrl Pts',(45.6605461902927,-4.09289113698077,332.269383729131));
#29670=CARTESIAN_POINT('Ctrl Pts',(45.652789080518,-4.16748880419008,332.384658600302));
#29671=CARTESIAN_POINT('Ctrl Pts',(45.6450319707433,-4.23709057543311,332.502752211318));
#29672=CARTESIAN_POINT('Ctrl Pts',(45.6372707158171,-4.30672953963721,332.620908927784));
#29673=CARTESIAN_POINT('Ctrl Pts',(45.6295094608909,-4.37136710425829,332.741887040846));
#29674=CARTESIAN_POINT('Ctrl Pts',(45.6217482059647,-4.43078870617346,332.865217925936));
#29675=CARTESIAN_POINT('Ctrl Pts',(45.61397453556,-4.49030536328627,332.988746100249));
#29676=CARTESIAN_POINT('Ctrl Pts',(45.6062008651553,-4.54458922937574,333.114634208398));
#29677=CARTESIAN_POINT('Ctrl Pts',(45.5984271947507,-4.59347418815556,333.242394257733));
#29678=CARTESIAN_POINT('Ctrl Pts',(45.5910153905738,-4.64008354034179,333.364207046031));
#29679=CARTESIAN_POINT('Ctrl Pts',(45.5836035863969,-4.68178521986609,333.487721147128));
#29680=CARTESIAN_POINT('Ctrl Pts',(45.57619178222,-4.71847830955698,333.612503872171));
#29681=CARTESIAN_POINT('Ctrl Pts',(45.5665478765862,-4.76622170454504,333.774865531535));
#29682=CARTESIAN_POINT('Ctrl Pts',(45.5569039709524,-4.80560894877283,333.939788460419));
#29683=CARTESIAN_POINT('Ctrl Pts',(45.5472600653186,-4.83640864842891,334.106504366042));
#29684=CARTESIAN_POINT('Ctrl Pts',(45.537753019719,-4.86677125878656,334.270854348002));
#29685=CARTESIAN_POINT('Ctrl Pts',(45.5282459741194,-4.88878833469871,334.436946835478));
#29686=CARTESIAN_POINT('Ctrl Pts',(45.5187389285197,-4.90228382780651,334.604024831427));
#29687=CARTESIAN_POINT('Ctrl Pts',(45.5113380351879,-4.91278958418529,334.734089046766));
#29688=CARTESIAN_POINT('Ctrl Pts',(45.503937141856,-4.91813207402702,334.864750086541));
#29689=CARTESIAN_POINT('Ctrl Pts',(45.4965362485241,-4.91824806876705,334.995641494621));
#29690=CARTESIAN_POINT('',(48.9965362484528,-4.91824811618257,335.004304668006));
#29691=CARTESIAN_POINT('Ctrl Pts',(48.9965362484528,-4.91824811618257,335.004304668006));
#29692=CARTESIAN_POINT('Ctrl Pts',(48.9871270537799,-4.91810243521494,335.170750754804));
#29693=CARTESIAN_POINT('Ctrl Pts',(48.977717859107,-4.90950360885218,335.336825553689));
#29694=CARTESIAN_POINT('Ctrl Pts',(48.9683086644341,-4.89258686062691,335.501773727611));
#29695=CARTESIAN_POINT('Ctrl Pts',(48.9587672542104,-4.8754324026652,335.669039710277));
#29696=CARTESIAN_POINT('Ctrl Pts',(48.9492258439866,-4.84972467282967,335.835147204582));
#29697=CARTESIAN_POINT('Ctrl Pts',(48.9396844337628,-4.81565367945835,335.999331127314));
#29698=CARTESIAN_POINT('Ctrl Pts',(48.9314723536777,-4.78632953139384,336.140640586876));
#29699=CARTESIAN_POINT('Ctrl Pts',(48.9232602735926,-4.75081098049385,336.280525521972));
#29700=CARTESIAN_POINT('Ctrl Pts',(48.9150481935074,-4.7092472580705,336.418510953379));
#29701=CARTESIAN_POINT('Ctrl Pts',(48.907273114729,-4.66989532618284,336.549153566254));
#29702=CARTESIAN_POINT('Ctrl Pts',(48.8994980359506,-4.62504071553603,336.678363843504));
#29703=CARTESIAN_POINT('Ctrl Pts',(48.8917229571721,-4.57480440138443,336.80564330685));
#29704=CARTESIAN_POINT('Ctrl Pts',(48.8839574461231,-4.52462990621563,336.932766144714));
#29705=CARTESIAN_POINT('Ctrl Pts',(48.8761919350741,-4.46908702660577,337.057962536106));
#29706=CARTESIAN_POINT('Ctrl Pts',(48.8684264240251,-4.40834686517368,337.180747802662));
#29707=CARTESIAN_POINT('Ctrl Pts',(48.8606686125029,-4.34766692778848,337.303411327267));
#29708=CARTESIAN_POINT('Ctrl Pts',(48.8529108009808,-4.28180013577821,337.423668136446));
#29709=CARTESIAN_POINT('Ctrl Pts',(48.8451529894586,-4.21096602923657,337.541052569924));
#29710=CARTESIAN_POINT('Ctrl Pts',(48.8374010159355,-4.14018522760629,337.658348667893));
#29711=CARTESIAN_POINT('Ctrl Pts',(48.8296490424125,-4.06444475300885,337.772776359314));
#29712=CARTESIAN_POINT('Ctrl Pts',(48.8218970688895,-3.98401034221723,337.88389400908));
#29713=CARTESIAN_POINT('Ctrl Pts',(48.8141483783318,-3.90360999544645,337.994964600455));
#29714=CARTESIAN_POINT('Ctrl Pts',(48.8063996877743,-3.8185198949626,338.1027276223));
#29715=CARTESIAN_POINT('Ctrl Pts',(48.7986509972167,-3.72904929426316,338.206770092079));
#29716=CARTESIAN_POINT('Ctrl Pts',(48.7909039188388,-3.63959730866947,338.310790914954));
#29717=CARTESIAN_POINT('Ctrl Pts',(48.783156840461,-3.54576689039424,338.411092429311));
#29718=CARTESIAN_POINT('Ctrl Pts',(48.7754097620831,-3.44790755166998,338.507294766289));
#29719=CARTESIAN_POINT('Ctrl Pts',(48.7676626187773,-3.35004739279028,338.603497909535));
#29720=CARTESIAN_POINT('Ctrl Pts',(48.7599154754716,-3.24815852485193,338.69560153286));
#29721=CARTESIAN_POINT('Ctrl Pts',(48.7521683321658,-3.1426269951272,338.78326296099));
#29722=CARTESIAN_POINT('Ctrl Pts',(48.7444194471377,-3.03707173967402,338.87094409727));
#29723=CARTESIAN_POINT('Ctrl Pts',(48.7366705621096,-2.92787249343328,338.954180801344));
#29724=CARTESIAN_POINT('Ctrl Pts',(48.7289216770815,-2.81544769328122,339.032671242353));
#29725=CARTESIAN_POINT('Ctrl Pts',(48.7211645673068,-2.70290356428479,339.111244993926));
#29726=CARTESIAN_POINT('Ctrl Pts',(48.713407457532,-2.58712736334224,339.185062194982));
#29727=CARTESIAN_POINT('Ctrl Pts',(48.7056503477573,-2.46856623771255,339.253864571484));
#29728=CARTESIAN_POINT('Ctrl Pts',(48.6978890928312,-2.34994175680825,339.322703713776));
#29729=CARTESIAN_POINT('Ctrl Pts',(48.690127837905,-2.22852973170751,339.386522510074));
#29730=CARTESIAN_POINT('Ctrl Pts',(48.6823665829789,-2.10480022581093,339.445109568045));
#29731=CARTESIAN_POINT('Ctrl Pts',(48.6745929125742,-1.98087279302818,339.503790346215));
#29732=CARTESIAN_POINT('Ctrl Pts',(48.6668192421695,-1.85462083149161,339.557222509742));
#29733=CARTESIAN_POINT('Ctrl Pts',(48.6590455717649,-1.72653344494976,339.605243242867));
#29734=CARTESIAN_POINT('Ctrl Pts',(48.6516337675877,-1.60440855706575,339.651028599312));
#29735=CARTESIAN_POINT('Ctrl Pts',(48.6442219634105,-1.48061555003002,339.691894901509));
#29736=CARTESIAN_POINT('Ctrl Pts',(48.6368101592333,-1.3555877845884,339.727744157711));
#29737=CARTESIAN_POINT('Ctrl Pts',(48.6290350804549,-1.22443203592577,339.765350492749));
#29738=CARTESIAN_POINT('Ctrl Pts',(48.6212600016764,-1.09150295362755,339.797554388829));
#29739=CARTESIAN_POINT('Ctrl Pts',(48.613484922898,-0.957285185365169,339.824187821425));
#29740=CARTESIAN_POINT('Ctrl Pts',(48.605719411849,-0.823232580611261,339.850788479886));
#29741=CARTESIAN_POINT('Ctrl Pts',(48.5979539007999,-0.68789482493425,339.871832238616));
#29742=CARTESIAN_POINT('Ctrl Pts',(48.5901883897509,-0.551772088158436,
339.887200694184));
#29743=CARTESIAN_POINT('Ctrl Pts',(48.5824305782287,-0.415784317472539,
339.902553911882));
#29744=CARTESIAN_POINT('Ctrl Pts',(48.5746727667066,-0.27901350047548,339.912242981055));
#29745=CARTESIAN_POINT('Ctrl Pts',(48.5669149551844,-0.141970026566872,
339.916200522157));
#29746=CARTESIAN_POINT('Ctrl Pts',(48.5591629816614,-0.00502968221827982,
339.920155085084));
#29747=CARTESIAN_POINT('Ctrl Pts',(48.5514110081383,0.132182521496973,339.91838669383));
#29748=CARTESIAN_POINT('Ctrl Pts',(48.5436590346153,0.26915139878126,339.91087981802));
#29749=CARTESIAN_POINT('Ctrl Pts',(48.5359103440577,0.406062269664699,339.903376121376));
#29750=CARTESIAN_POINT('Ctrl Pts',(48.5281616535001,0.542729629597855,339.890138795123));
#29751=CARTESIAN_POINT('Ctrl Pts',(48.5204129629425,0.678638837944847,339.871204408576));
#29752=CARTESIAN_POINT('Ctrl Pts',(48.5126658845646,0.814519769245907,339.852273961487));
#29753=CARTESIAN_POINT('Ctrl Pts',(48.5049188061868,0.949642475824041,339.827648865693));
#29754=CARTESIAN_POINT('Ctrl Pts',(48.497171727809,1.08349837672737,339.79741746465));
#29755=CARTESIAN_POINT('Ctrl Pts',(48.4894245845032,1.21735539947198,339.767185810239));
#29756=CARTESIAN_POINT('Ctrl Pts',(48.4816774411973,1.34994521409406,339.731347842972));
#29757=CARTESIAN_POINT('Ctrl Pts',(48.4739302978915,1.48077074531474,339.690042756982));
#29758=CARTESIAN_POINT('Ctrl Pts',(48.4661814128635,1.61162568889215,339.648728384732));
#29759=CARTESIAN_POINT('Ctrl Pts',(48.4584325278354,1.74071518711738,339.6019445656));
#29760=CARTESIAN_POINT('Ctrl Pts',(48.4506836428073,1.86755898377751,339.549879834085));
#29761=CARTESIAN_POINT('Ctrl Pts',(48.4429265330326,1.99453741375413,339.497759840525));
#29762=CARTESIAN_POINT('Ctrl Pts',(48.4351694232578,2.1192650185099,339.440347886297));
#29763=CARTESIAN_POINT('Ctrl Pts',(48.4274123134831,2.24128263285874,339.377880220169));
#29764=CARTESIAN_POINT('Ctrl Pts',(48.4196510585569,2.36336544951923,339.315379173317));
#29765=CARTESIAN_POINT('Ctrl Pts',(48.4118898036308,2.48273505024341,339.247817223797));
#29766=CARTESIAN_POINT('Ctrl Pts',(48.4041285487046,2.5989592924295,339.175475261428));
#29767=CARTESIAN_POINT('Ctrl Pts',(48.3963548782999,2.71536945552577,339.103017575495));
#29768=CARTESIAN_POINT('Ctrl Pts',(48.3885812078953,2.82862388248384,339.025764817192));
#29769=CARTESIAN_POINT('Ctrl Pts',(48.3808075374907,2.9383209759564,338.944040175347));
#29770=CARTESIAN_POINT('Ctrl Pts',(48.3733957333136,3.04291164333591,338.866119835243));
#29771=CARTESIAN_POINT('Ctrl Pts',(48.3659839291365,3.14426848804456,338.784134755646));
#29772=CARTESIAN_POINT('Ctrl Pts',(48.3585721249594,3.24207459036566,338.698396329898));
#29773=CARTESIAN_POINT('Ctrl Pts',(48.350797046181,3.34467446111122,338.608455608502));
#29774=CARTESIAN_POINT('Ctrl Pts',(48.3430219674025,3.44369095826579,338.514100083308));
#29775=CARTESIAN_POINT('Ctrl Pts',(48.3352468886241,3.53872051575556,338.415646377169));
#29776=CARTESIAN_POINT('Ctrl Pts',(48.3274813775751,3.63363313332503,338.317313824584));
#29777=CARTESIAN_POINT('Ctrl Pts',(48.3197158665261,3.72456830426629,338.21489340387));
#29778=CARTESIAN_POINT('Ctrl Pts',(48.3119503554771,3.81115579001483,338.108741643613));
#29779=CARTESIAN_POINT('Ctrl Pts',(48.3041925439548,3.8976574240191,338.002695133136));
#29780=CARTESIAN_POINT('Ctrl Pts',(48.2964347324327,3.9798197059786,337.892924946534));
#29781=CARTESIAN_POINT('Ctrl Pts',(48.2886769209105,4.0573097740065,337.779823818203));
#29782=CARTESIAN_POINT('Ctrl Pts',(48.2809249473874,4.13474152830081,337.666807802059));
#29783=CARTESIAN_POINT('Ctrl Pts',(48.2731729738644,4.20750784703314,337.550466154683));
#29784=CARTESIAN_POINT('Ctrl Pts',(48.2654210003414,4.27531687378358,337.431223702427));
#29785=CARTESIAN_POINT('Ctrl Pts',(48.2576723097838,4.34309718337099,337.31203174942));
#29786=CARTESIAN_POINT('Ctrl Pts',(48.2499236192262,4.40592418374961,337.189941773988));
#29787=CARTESIAN_POINT('Ctrl Pts',(48.2421749286685,4.46355012526062,337.065406338178));
#29788=CARTESIAN_POINT('Ctrl Pts',(48.2344278502907,4.52116407721321,336.940896813006));
#29789=CARTESIAN_POINT('Ctrl Pts',(48.2266807719128,4.57357895867524,336.813943194006));
#29790=CARTESIAN_POINT('Ctrl Pts',(48.218933693535,4.62059383720838,336.685020965464));
#29791=CARTESIAN_POINT('Ctrl Pts',(48.2111865502292,4.66760910977145,336.556097656429));
#29792=CARTESIAN_POINT('Ctrl Pts',(48.2034394069234,4.7092241552209,336.425206072164));
#29793=CARTESIAN_POINT('Ctrl Pts',(48.1956922636176,4.74528702891783,336.292839539805));
#29794=CARTESIAN_POINT('Ctrl Pts',(48.1879433785895,4.78135801031437,336.160443248641));
#29795=CARTESIAN_POINT('Ctrl Pts',(48.1801944935614,4.81187423336076,336.026571726592));
#29796=CARTESIAN_POINT('Ctrl Pts',(48.1724456085333,4.83673434654541,335.89173085819));
#29797=CARTESIAN_POINT('Ctrl Pts',(48.1646884987586,4.86162084651107,335.756746868297));
#29798=CARTESIAN_POINT('Ctrl Pts',(48.1569313889838,4.88083917317195,335.620791861781));
#29799=CARTESIAN_POINT('Ctrl Pts',(48.1491742792091,4.89433951252887,335.484379808207));
#29800=CARTESIAN_POINT('Ctrl Pts',(48.1414130242829,4.90784706603548,335.347894860394));
#29801=CARTESIAN_POINT('Ctrl Pts',(48.1336517693567,4.91563052169075,335.210952768916));
#29802=CARTESIAN_POINT('Ctrl Pts',(48.1258905144306,4.91769222857898,335.074068937308));
#29803=CARTESIAN_POINT('Ctrl Pts',(48.1181168440259,4.91975723352632,334.936966136179));
#29804=CARTESIAN_POINT('Ctrl Pts',(48.1103431736212,4.91608220991886,334.799922172092));
#29805=CARTESIAN_POINT('Ctrl Pts',(48.1025695032166,4.90672160676861,334.663449652845));
#29806=CARTESIAN_POINT('Ctrl Pts',(48.0951576990396,4.89779674194713,334.533329962204));
#29807=CARTESIAN_POINT('Ctrl Pts',(48.0877458948625,4.88370374396625,334.403729998264));
#29808=CARTESIAN_POINT('Ctrl Pts',(48.0803340906855,4.8645329666847,334.275084778379));
#29809=CARTESIAN_POINT('Ctrl Pts',(48.0725590119071,4.84442257250159,334.140134273052));
#29810=CARTESIAN_POINT('Ctrl Pts',(48.0647839331287,4.81866050655486,334.00580799937));
#29811=CARTESIAN_POINT('Ctrl Pts',(48.0570088543503,4.78729463099764,333.872616667446));
#29812=CARTESIAN_POINT('Ctrl Pts',(48.0492433433013,4.75596735314714,333.739589235935));
#29813=CARTESIAN_POINT('Ctrl Pts',(48.0414778322522,4.71905007518084,333.607694344144));
#29814=CARTESIAN_POINT('Ctrl Pts',(48.0337123212032,4.67664225225996,333.477436271653));
#29815=CARTESIAN_POINT('Ctrl Pts',(48.025954509681,4.63427647681895,333.347307350421));
#29816=CARTESIAN_POINT('Ctrl Pts',(48.0181966981588,4.5864311103,333.218812388084));
#29817=CARTESIAN_POINT('Ctrl Pts',(48.0104388866366,4.53325628076957,333.09244382642));
#29818=CARTESIAN_POINT('Ctrl Pts',(48.0026869131136,4.48012146698467,332.966170361107));
#29819=CARTESIAN_POINT('Ctrl Pts',(47.9949349395906,4.42166532406268,332.842020470206));
#29820=CARTESIAN_POINT('Ctrl Pts',(47.9871829660676,4.35808715729016,332.720469479923));
#29821=CARTESIAN_POINT('Ctrl Pts',(47.97943427551,4.29453591590902,332.598969966557));
#29822=CARTESIAN_POINT('Ctrl Pts',(47.9716855849524,4.22586714581079,332.480067510356));
#29823=CARTESIAN_POINT('Ctrl Pts',(47.9639368943948,4.15232734451882,332.364215356585));
#29824=CARTESIAN_POINT('Ctrl Pts',(47.9561898160169,4.07880284379672,332.248387306823));
#29825=CARTESIAN_POINT('Ctrl Pts',(47.9484427376391,4.0004095370675,332.135608626941));
#29826=CARTESIAN_POINT('Ctrl Pts',(47.9406956592613,3.91743853313924,332.026305597144));
#29827=CARTESIAN_POINT('Ctrl Pts',(47.9329485159555,3.8344668338341,331.917001651283));
#29828=CARTESIAN_POINT('Ctrl Pts',(47.9252013726497,3.74691759713921,331.811173724943));
#29829=CARTESIAN_POINT('Ctrl Pts',(47.9174542293439,3.65512344640808,331.709216559234));
#29830=CARTESIAN_POINT('Ctrl Pts',(47.9097053443158,3.56330865840308,331.607236471391));
#29831=CARTESIAN_POINT('Ctrl Pts',(47.9019564592877,3.46724731879979,331.509129166269));
#29832=CARTESIAN_POINT('Ctrl Pts',(47.8942075742596,3.36730998957424,331.415253635665));
#29833=CARTESIAN_POINT('Ctrl Pts',(47.8864504644849,3.26726658583476,331.321278464603));
#29834=CARTESIAN_POINT('Ctrl Pts',(47.8786933547102,3.16333925968627,331.231544308586));
#29835=CARTESIAN_POINT('Ctrl Pts',(47.8709362449354,3.05593326188828,331.146371195693));
#29836=CARTESIAN_POINT('Ctrl Pts',(47.8631749900093,2.94846986975925,331.061152569012));
#29837=CARTESIAN_POINT('Ctrl Pts',(47.8554137350832,2.83752441797451,330.980500071664));
#29838=CARTESIAN_POINT('Ctrl Pts',(47.847652480157,2.72353159158441,330.904690642681));
#29839=CARTESIAN_POINT('Ctrl Pts',(47.8398788097523,2.60935641382235,330.828759943318));
#29840=CARTESIAN_POINT('Ctrl Pts',(47.8321051393476,2.49212445457095,330.757687996525));
#29841=CARTESIAN_POINT('Ctrl Pts',(47.824331468943,2.37229624214689,330.691706416457));
#29842=CARTESIAN_POINT('Ctrl Pts',(47.8169196647658,2.2580460618388,330.628796294815));
#29843=CARTESIAN_POINT('Ctrl Pts',(47.8095078605886,2.14143615740147,330.570513420545));
#29844=CARTESIAN_POINT('Ctrl Pts',(47.8020960564115,2.02288123986652,330.517017226009));
#29845=CARTESIAN_POINT('Ctrl Pts',(47.794320977633,1.89851559266764,330.460899023624));
#29846=CARTESIAN_POINT('Ctrl Pts',(47.7865458988546,1.77161643129144,330.409871240158));
#29847=CARTESIAN_POINT('Ctrl Pts',(47.7787708200762,1.64263912372649,330.364170001855));
#29848=CARTESIAN_POINT('Ctrl Pts',(47.7710053090272,1.51382053094959,330.318525001835));
#29849=CARTESIAN_POINT('Ctrl Pts',(47.7632397979782,1.38292924516727,330.278193634396));
#29850=CARTESIAN_POINT('Ctrl Pts',(47.7554742869292,1.25044314673299,330.243365160191));
#29851=CARTESIAN_POINT('Ctrl Pts',(47.747716475407,1.11808840865112,330.208571218518));
#29852=CARTESIAN_POINT('Ctrl Pts',(47.7399586638847,0.984142380311724,330.1792694108));
#29853=CARTESIAN_POINT('Ctrl Pts',(47.7322008523626,0.849100409423858,330.155599979645));
#29854=CARTESIAN_POINT('Ctrl Pts',(47.7244488788395,0.714160061901511,330.131948360487));
#29855=CARTESIAN_POINT('Ctrl Pts',(47.7166969053165,0.578125796873363,330.113920748492));
#29856=CARTESIAN_POINT('Ctrl Pts',(47.7089449317935,0.441505181812714,330.101606769875));
#29857=CARTESIAN_POINT('Ctrl Pts',(47.7011962412359,0.304942425663562,330.089298006236));
#29858=CARTESIAN_POINT('Ctrl Pts',(47.6934475506783,0.167794201858067,330.082698098324));
#29859=CARTESIAN_POINT('Ctrl Pts',(47.6856988601207,0.0305750479628804,
330.081845038132));
#29860=CARTESIAN_POINT('Ctrl Pts',(47.6779517817429,-0.106615556341168,
330.080992155428));
#29861=CARTESIAN_POINT('Ctrl Pts',(47.670204703365,-0.243876670759664,330.085883744581));
#29862=CARTESIAN_POINT('Ctrl Pts',(47.6624576249872,-0.380692291494497,
330.096505690663));
#29863=CARTESIAN_POINT('Ctrl Pts',(47.6547104816814,-0.517509058875916,
330.107127725768));
#29864=CARTESIAN_POINT('Ctrl Pts',(47.6469633383756,-0.653879935425003,
330.123480183338));
#29865=CARTESIAN_POINT('Ctrl Pts',(47.6392161950698,-0.789292973337843,
330.145496970365));
#29866=CARTESIAN_POINT('Ctrl Pts',(47.6314673100417,-0.9247364549766,330.167518707232));
#29867=CARTESIAN_POINT('Ctrl Pts',(47.6237184250137,-1.05922128373901,330.195207244886));
#29868=CARTESIAN_POINT('Ctrl Pts',(47.6159695399856,-1.19224504341742,330.228445240915));
#29869=CARTESIAN_POINT('Ctrl Pts',(47.6082124302108,-1.32540999588875,330.261718516096));
#29870=CARTESIAN_POINT('Ctrl Pts',(47.6004553204361,-1.45711040160517,330.300552921081));
#29871=CARTESIAN_POINT('Ctrl Pts',(47.5926982106614,-1.58685783768899,330.344780857418));
#29872=CARTESIAN_POINT('Ctrl Pts',(47.5849369557352,-1.71667460665414,330.389032427749));
#29873=CARTESIAN_POINT('Ctrl Pts',(47.577175700809,-1.84453596232846,330.438683130918));
#29874=CARTESIAN_POINT('Ctrl Pts',(47.5694144458829,-1.96997378775028,330.493517298593));
#29875=CARTESIAN_POINT('Ctrl Pts',(47.5616407754782,-2.09561227281259,330.548439183066));
#29876=CARTESIAN_POINT('Ctrl Pts',(47.5538671050736,-2.21881912904405,330.608560930118));
#29877=CARTESIAN_POINT('Ctrl Pts',(47.5460934346689,-2.33915036886212,330.673620611371));
#29878=CARTESIAN_POINT('Ctrl Pts',(47.5386816304918,-2.45388016051664,330.73565174881));
#29879=CARTESIAN_POINT('Ctrl Pts',(47.5312698263147,-2.56599578326613,330.802171297675));
#29880=CARTESIAN_POINT('Ctrl Pts',(47.5238580221376,-2.67513874309868,330.872916796614));
#29881=CARTESIAN_POINT('Ctrl Pts',(47.516087547911,-2.78956331991435,330.947085792856));
#29882=CARTESIAN_POINT('Ctrl Pts',(47.5083170736843,-2.90108290454413,331.026134975483));
#29883=CARTESIAN_POINT('Ctrl Pts',(47.5005465994576,-3.00925281587577,331.109809702258));
#29884=CARTESIAN_POINT('Ctrl Pts',(47.4927856906637,-3.11728957033832,331.193381425671));
#29885=CARTESIAN_POINT('Ctrl Pts',(47.4850247818698,-3.22198454916022,331.281567126827));
#29886=CARTESIAN_POINT('Ctrl Pts',(47.477263873076,-3.32292027247217,331.37406785429));
#29887=CARTESIAN_POINT('Ctrl Pts',(47.4695106565121,-3.42375595327387,331.466476899595));
#29888=CARTESIAN_POINT('Ctrl Pts',(47.4617574399482,-3.52083950663695,331.563192197508));
#29889=CARTESIAN_POINT('Ctrl Pts',(47.4540042233843,-3.6137852015038,331.663873566561));
#29890=CARTESIAN_POINT('Ctrl Pts',(47.4462568325578,-3.70666105732902,331.764479284016));
#29891=CARTESIAN_POINT('Ctrl Pts',(47.4385094417314,-3.79540497875993,331.869044854578));
#29892=CARTESIAN_POINT('Ctrl Pts',(47.4307620509049,-3.87966717411193,331.977192417533));
#29893=CARTESIAN_POINT('Ctrl Pts',(47.4230179225773,-3.96389388586381,332.085294438536));
#29894=CARTESIAN_POINT('Ctrl Pts',(47.4152737942498,-4.04364238505329,332.196975143799));
#29895=CARTESIAN_POINT('Ctrl Pts',(47.4075296659222,-4.1186025216092,332.311822860842));
#29896=CARTESIAN_POINT('Ctrl Pts',(47.399787129472,-4.19354724941406,332.426646969871));
#29897=CARTESIAN_POINT('Ctrl Pts',(47.3920445930219,-4.26370535857375,332.544636468245));
#29898=CARTESIAN_POINT('Ctrl Pts',(47.3843020565717,-4.32880972192682,332.665350250283));
#29899=CARTESIAN_POINT('Ctrl Pts',(47.3765594304384,-4.39391483939484,332.78606543057));
#29900=CARTESIAN_POINT('Ctrl Pts',(47.368816804305,-4.45396590860242,332.909504612914));
#29901=CARTESIAN_POINT('Ctrl Pts',(47.3610741781717,-4.5087417087322,333.035201978208));
#29902=CARTESIAN_POINT('Ctrl Pts',(47.3533297810897,-4.56353003757391,333.1609280939));
#29903=CARTESIAN_POINT('Ctrl Pts',(47.3455853840077,-4.61304054009972,333.288913061565));
#29904=CARTESIAN_POINT('Ctrl Pts',(47.3378409869257,-4.65710025417135,333.418671354494));
#29905=CARTESIAN_POINT('Ctrl Pts',(47.3300883647611,-4.70120676269058,333.548567459658));
#29906=CARTESIAN_POINT('Ctrl Pts',(47.3223357425966,-4.73985079285584,333.68024028102));
#29907=CARTESIAN_POINT('Ctrl Pts',(47.3145831204321,-4.77290922257903,333.81318888802));
#29908=CARTESIAN_POINT('Ctrl Pts',(47.3068263182969,-4.8059854763705,333.946209176738));
#29909=CARTESIAN_POINT('Ctrl Pts',(47.2990695161617,-4.83347005073907,334.080506238446));
#29910=CARTESIAN_POINT('Ctrl Pts',(47.2913127140265,-4.85529123749409,334.215570231561));
#29911=CARTESIAN_POINT('Ctrl Pts',(47.283543580039,-4.87714711581998,334.350848950948));
#29912=CARTESIAN_POINT('Ctrl Pts',(47.2757744460515,-4.89332156925475,334.486896649303));
#29913=CARTESIAN_POINT('Ctrl Pts',(47.2680053120641,-4.90379484877796,334.623198800959));
#29914=CARTESIAN_POINT('Ctrl Pts',(47.2608489575514,-4.91344206316505,334.748750312836));
#29915=CARTESIAN_POINT('Ctrl Pts',(47.2536926030387,-4.91825257170291,334.874517465928));
#29916=CARTESIAN_POINT('Ctrl Pts',(47.246536248526,-4.91824999896793,335.000100756667));
#29917=CARTESIAN_POINT('',(50.7465362485347,-4.9182495281824,334.997845694185));
#29918=CARTESIAN_POINT('Ctrl Pts',(50.7465362484901,-4.91824952818275,334.997845694977));
#29919=CARTESIAN_POINT('Ctrl Pts',(50.7386479016619,-4.91831084118688,335.137822462629));
#29920=CARTESIAN_POINT('Ctrl Pts',(50.7307595548337,-4.91239204902384,335.277775344747));
#29921=CARTESIAN_POINT('Ctrl Pts',(50.7228712080056,-4.90052569889815,335.417170153461));
#29922=CARTESIAN_POINT('Ctrl Pts',(50.7149796963707,-4.88865458798989,335.556620887407));
#29923=CARTESIAN_POINT('Ctrl Pts',(50.707088184736,-4.87083119616067,335.69551273247));
#29924=CARTESIAN_POINT('Ctrl Pts',(50.6991966731011,-4.84713987443125,335.833317526636));
#29925=CARTESIAN_POINT('Ctrl Pts',(50.6913005484341,-4.82343470379245,335.971202875451));
#29926=CARTESIAN_POINT('Ctrl Pts',(50.683404423767,-4.79385483167211,336.107999542287));
#29927=CARTESIAN_POINT('Ctrl Pts',(50.6755082991,-4.75853551509368,336.243190578348));
#29928=CARTESIAN_POINT('Ctrl Pts',(50.6676003404927,-4.72316326537386,336.378584225526));
#29929=CARTESIAN_POINT('Ctrl Pts',(50.6596923818854,-4.68203447918535,336.512367074974));
#29930=CARTESIAN_POINT('Ctrl Pts',(50.6517844232781,-4.63533431358539,336.64403736691));
#29931=CARTESIAN_POINT('Ctrl Pts',(50.6438702478799,-4.58859743494991,336.775811170602));
#29932=CARTESIAN_POINT('Ctrl Pts',(50.6359560724817,-4.53628058314284,336.905468762458));
#29933=CARTESIAN_POINT('Ctrl Pts',(50.6280418970835,-4.47861646679156,337.032529853627));
#29934=CARTESIAN_POINT('Ctrl Pts',(50.6201131041793,-4.42084584464198,337.159825627017));
#29935=CARTESIAN_POINT('Ctrl Pts',(50.612184311275,-4.35770838602701,337.28451498402));
#29936=CARTESIAN_POINT('Ctrl Pts',(50.6042555183708,-4.28948260207043,337.406142570388));
#29937=CARTESIAN_POINT('Ctrl Pts',(50.5976624786309,-4.23275072493055,337.50727971952));
#29938=CARTESIAN_POINT('Ctrl Pts',(50.5910694388909,-4.1725014178184,337.606300241126));
#29939=CARTESIAN_POINT('Ctrl Pts',(50.584476399151,-4.10891655614067,337.702959081668));
#29940=CARTESIAN_POINT('Ctrl Pts',(50.5767013203726,-4.03393182555143,337.816947489064));
#29941=CARTESIAN_POINT('Ctrl Pts',(50.5689262415942,-3.95408165905571,337.927993347852));
#29942=CARTESIAN_POINT('Ctrl Pts',(50.5611511628157,-3.86962420424877,338.035653402546));
#29943=CARTESIAN_POINT('Ctrl Pts',(50.5533856517667,-3.78527067971686,338.143180974689));
#29944=CARTESIAN_POINT('Ctrl Pts',(50.5456201407177,-3.69632138662564,338.247330728178));
#29945=CARTESIAN_POINT('Ctrl Pts',(50.5378546296687,-3.60307858040679,338.347686933677));
#29946=CARTESIAN_POINT('Ctrl Pts',(50.5300968181464,-3.50992822470139,338.447943635707));
#29947=CARTESIAN_POINT('Ctrl Pts',(50.5223390066242,-3.41249309194134,338.544413990468));
#29948=CARTESIAN_POINT('Ctrl Pts',(50.514581195102,-3.31111643715103,338.636714314065));
#29949=CARTESIAN_POINT('Ctrl Pts',(50.506829221579,-3.20981607150857,338.728945178742));
#29950=CARTESIAN_POINT('Ctrl Pts',(50.499077248056,-3.10458037561479,338.817011996363));
#29951=CARTESIAN_POINT('Ctrl Pts',(50.491325274533,-2.99579002805088,338.900567288271));
#29952=CARTESIAN_POINT('Ctrl Pts',(50.4835765839753,-2.8870457532639,338.984087194464));
#29953=CARTESIAN_POINT('Ctrl Pts',(50.4758278934177,-2.77475013028511,339.063099137468));
#29954=CARTESIAN_POINT('Ctrl Pts',(50.4680792028601,-2.65931737261189,339.137295514491));
#29955=CARTESIAN_POINT('Ctrl Pts',(50.4603321244822,-2.54390863168793,339.211476454338));
#29956=CARTESIAN_POINT('Ctrl Pts',(50.4525850461044,-2.42536438295216,339.280843609877));
#29957=CARTESIAN_POINT('Ctrl Pts',(50.4448379677266,-2.30412797960113,339.345132600522));
#29958=CARTESIAN_POINT('Ctrl Pts',(50.4370908244207,-2.18289056017243,339.409422129971));
#29959=CARTESIAN_POINT('Ctrl Pts',(50.429343681115,-2.05896128645139,339.468633226518));
#29960=CARTESIAN_POINT('Ctrl Pts',(50.4215965378092,-1.93280791850323,339.522547579923));
#29961=CARTESIAN_POINT('Ctrl Pts',(50.4138476527811,-1.80662618859973,339.57647405442));
#29962=CARTESIAN_POINT('Ctrl Pts',(50.406098767753,-1.6782197288339,339.625101262596));
#29963=CARTESIAN_POINT('Ctrl Pts',(50.3983498827249,-1.54807569149528,339.668259281135));
#29964=CARTESIAN_POINT('Ctrl Pts',(50.3905927729502,-1.41779351793071,339.71146310804));
#29965=CARTESIAN_POINT('Ctrl Pts',(50.3828356631754,-1.2857704542579,339.74918602594));
#29966=CARTESIAN_POINT('Ctrl Pts',(50.3750785534007,-1.15250874488829,339.781308048584));
#29967=CARTESIAN_POINT('Ctrl Pts',(50.3673172984745,-1.019175824722,339.813447236211));
#29968=CARTESIAN_POINT('Ctrl Pts',(50.3595560435484,-0.884603323275451,
339.83997948931));
#29969=CARTESIAN_POINT('Ctrl Pts',(50.3517947886222,-0.749302075125627,
339.860836292523));
#29970=CARTESIAN_POINT('Ctrl Pts',(50.3440211182175,-0.613784389073338,
339.881726459825));
#29971=CARTESIAN_POINT('Ctrl Pts',(50.3362474478128,-0.477536015459398,
339.896922991618));
#29972=CARTESIAN_POINT('Ctrl Pts',(50.3284737774082,-0.34107218078802,339.906409362252));
#29973=CARTESIAN_POINT('Ctrl Pts',(50.3210619732311,-0.210960770451982,
339.91545414005));
#29974=CARTESIAN_POINT('Ctrl Pts',(50.313650169054,-0.080653794728576,339.919308400497));
#29975=CARTESIAN_POINT('Ctrl Pts',(50.3062383648769,0.0494054387711424,
339.918001846799));
#29976=CARTESIAN_POINT('Ctrl Pts',(50.2984632860985,0.185839262731332,339.916631255013));
#29977=CARTESIAN_POINT('Ctrl Pts',(50.29068820732,0.322431601338373,339.909576832478));
#29978=CARTESIAN_POINT('Ctrl Pts',(50.2829131285416,0.458670013120958,339.896815790038));
#29979=CARTESIAN_POINT('Ctrl Pts',(50.2751476174925,0.594740774864668,339.884070450872));
#29980=CARTESIAN_POINT('Ctrl Pts',(50.2673821064435,0.730458090912218,339.865632500386));
#29981=CARTESIAN_POINT('Ctrl Pts',(50.2596165953945,0.865308797838984,339.841531136622));
#29982=CARTESIAN_POINT('Ctrl Pts',(50.2518587838723,1.00002579989732,339.817453669431));
#29983=CARTESIAN_POINT('Ctrl Pts',(50.24410097235,1.13387752048345,339.787724032034));
#29984=CARTESIAN_POINT('Ctrl Pts',(50.2363431608278,1.26635555663571,339.752423241535));
#29985=CARTESIAN_POINT('Ctrl Pts',(50.2285911873048,1.39873389886383,339.717149016));
#29986=CARTESIAN_POINT('Ctrl Pts',(50.2208392137819,1.52974023809469,339.676312082505));
#29987=CARTESIAN_POINT('Ctrl Pts',(50.2130872402589,1.65887636508962,339.630044521152));
#29988=CARTESIAN_POINT('Ctrl Pts',(50.2053385497013,1.78795780285853,339.583796554138));
#29989=CARTESIAN_POINT('Ctrl Pts',(50.1975898591436,1.91517023649173,339.532122665117));
#29990=CARTESIAN_POINT('Ctrl Pts',(50.189841168586,2.04003084154797,339.475204713534));
#29991=CARTESIAN_POINT('Ctrl Pts',(50.1820940902081,2.16486546831238,339.418298604206));
#29992=CARTESIAN_POINT('Ctrl Pts',(50.1743470118303,2.2873488843468,339.356150764562));
#29993=CARTESIAN_POINT('Ctrl Pts',(50.1665999334525,2.40701884252234,339.288990948258));
#29994=CARTESIAN_POINT('Ctrl Pts',(50.1588527901467,2.52668980364707,339.221830569091));
#29995=CARTESIAN_POINT('Ctrl Pts',(50.1511056468409,2.64354691901748,339.149658320778));
#29996=CARTESIAN_POINT('Ctrl Pts',(50.1433585035352,2.75715347508346,339.072749412539));
#29997=CARTESIAN_POINT('Ctrl Pts',(50.1356096185071,2.87078557231525,338.995823213544));
#29998=CARTESIAN_POINT('Ctrl Pts',(50.1278607334789,2.98116533242721,338.914158454669));
#29999=CARTESIAN_POINT('Ctrl Pts',(50.1201118484508,3.08788623721916,338.828072837407));
#30000=CARTESIAN_POINT('Ctrl Pts',(50.1123547386761,3.1947204166823,338.741895847982));
#30001=CARTESIAN_POINT('Ctrl Pts',(50.1045976289014,3.29788767836247,338.651288872566));
#30002=CARTESIAN_POINT('Ctrl Pts',(50.0968405191267,3.39701532999277,338.556609327758));
#30003=CARTESIAN_POINT('Ctrl Pts',(50.0890792642005,3.49619595227048,338.461879189228));
#30004=CARTESIAN_POINT('Ctrl Pts',(50.0813180092743,3.5913323922436,338.363072426356));
#30005=CARTESIAN_POINT('Ctrl Pts',(50.0735567543482,3.68209059198383,338.260581533243));
#30006=CARTESIAN_POINT('Ctrl Pts',(50.0657830839435,3.77299397526568,338.157926688103));
#30007=CARTESIAN_POINT('Ctrl Pts',(50.0580094135389,3.85950487594716,338.05157623933));
#30008=CARTESIAN_POINT('Ctrl Pts',(50.0502357431342,3.9413305786295,337.941954508904));
#30009=CARTESIAN_POINT('Ctrl Pts',(50.0428239389572,4.01934727516536,337.837435696404));
#30010=CARTESIAN_POINT('Ctrl Pts',(50.0354121347801,4.09310498657809,337.729943542026));
#30011=CARTESIAN_POINT('Ctrl Pts',(50.0280003306031,4.16238879174328,337.619866906709));
#30012=CARTESIAN_POINT('Ctrl Pts',(50.0202252518246,4.23506840258589,337.504395087593));
#30013=CARTESIAN_POINT('Ctrl Pts',(50.0124501730462,4.30305414026398,337.385714123173));
#30014=CARTESIAN_POINT('Ctrl Pts',(50.0046750942678,4.36604952940482,337.264242603893));
#30015=CARTESIAN_POINT('Ctrl Pts',(49.9969095832188,4.42896739870875,337.142920563051));
#30016=CARTESIAN_POINT('Ctrl Pts',(49.9891440721698,4.4869069599596,337.018815143608));
#30017=CARTESIAN_POINT('Ctrl Pts',(49.9813785611207,4.53961506424028,336.892373676371));
#30018=CARTESIAN_POINT('Ctrl Pts',(49.9736207495985,4.59227090828222,336.766057576217));
#30019=CARTESIAN_POINT('Ctrl Pts',(49.9658629380764,4.63970546836064,336.637410396094));
#30020=CARTESIAN_POINT('Ctrl Pts',(49.9581051265542,4.68171174747052,336.506903505901));
#30021=CARTESIAN_POINT('Ctrl Pts',(49.9503531530312,4.72368641552299,336.376494826282));
#30022=CARTESIAN_POINT('Ctrl Pts',(49.9426011795082,4.76024081422956,336.244229592789));
#30023=CARTESIAN_POINT('Ctrl Pts',(49.9348492059852,4.79121640295882,336.110598236321));
#30024=CARTESIAN_POINT('Ctrl Pts',(49.9271005154276,4.82217887350806,335.97702347281));
#30025=CARTESIAN_POINT('Ctrl Pts',(49.91935182487,4.84756714510293,335.842084117013));
#30026=CARTESIAN_POINT('Ctrl Pts',(49.9116031343124,4.86727286322162,335.706284600884));
#30027=CARTESIAN_POINT('Ctrl Pts',(49.9038560559346,4.88697448140102,335.570513338979));
#30028=CARTESIAN_POINT('Ctrl Pts',(49.8961089775568,4.90099584169176,335.433882659294));
#30029=CARTESIAN_POINT('Ctrl Pts',(49.8883618991789,4.90928000040002,335.296905608186));
#30030=CARTESIAN_POINT('Ctrl Pts',(49.8806147558731,4.91756422853751,335.159927409079));
#30031=CARTESIAN_POINT('Ctrl Pts',(49.8728676125673,4.92011113559047,335.022603222922));
#30032=CARTESIAN_POINT('Ctrl Pts',(49.8651204692615,4.91691582010293,334.885449222956));
#30033=CARTESIAN_POINT('Ctrl Pts',(49.8573715842335,4.91371978624064,334.748264387859));
#30034=CARTESIAN_POINT('Ctrl Pts',(49.8496226992053,4.90477897004681,334.611250205781));
#30035=CARTESIAN_POINT('Ctrl Pts',(49.8418738141772,4.89014054316272,334.474920453059));
#30036=CARTESIAN_POINT('Ctrl Pts',(49.8341167044025,4.8754865789011,334.338445998528));
#30037=CARTESIAN_POINT('Ctrl Pts',(49.8263595946278,4.85512296529114,334.20265781378));
#30038=CARTESIAN_POINT('Ctrl Pts',(49.8186024848531,4.82914857640288,334.068062722322));
#30039=CARTESIAN_POINT('Ctrl Pts',(49.8108412299269,4.80316030763167,333.93339570755));
#30040=CARTESIAN_POINT('Ctrl Pts',(49.8030799750008,4.77155537937993,333.799923436608));
#30041=CARTESIAN_POINT('Ctrl Pts',(49.7953187200746,4.73448307039813,333.668139227016));
#30042=CARTESIAN_POINT('Ctrl Pts',(49.78754504967,4.69735145780381,333.536144205637));
#30043=CARTESIAN_POINT('Ctrl Pts',(49.7797713792653,4.65473510889653,333.405843013406));
#30044=CARTESIAN_POINT('Ctrl Pts',(49.7719977088606,4.60683243998393,333.277711425918));
#30045=CARTESIAN_POINT('Ctrl Pts',(49.7645859046835,4.56115965183345,333.155544394654));
#30046=CARTESIAN_POINT('Ctrl Pts',(49.7571741005063,4.51068173583416,333.035349788941));
#30047=CARTESIAN_POINT('Ctrl Pts',(49.7497622963291,4.45560938729194,332.917518775505));
#30048=CARTESIAN_POINT('Ctrl Pts',(49.7419872175507,4.39783777889631,332.7939125131));
#30049=CARTESIAN_POINT('Ctrl Pts',(49.7342121387723,4.33482740764643,332.672516776115));
#30050=CARTESIAN_POINT('Ctrl Pts',(49.7264370599938,4.26676983534172,332.553807400322));
#30051=CARTESIAN_POINT('Ctrl Pts',(49.7186715489448,4.1987960122124,332.435244103974));
#30052=CARTESIAN_POINT('Ctrl Pts',(49.7109060378958,4.12578753849365,332.319360927203));
#30053=CARTESIAN_POINT('Ctrl Pts',(49.7031405268468,4.04798359080069,332.206612824704));
#30054=CARTESIAN_POINT('Ctrl Pts',(49.6953827153246,3.97025678594811,332.093976512276));
#30055=CARTESIAN_POINT('Ctrl Pts',(49.6876249038024,3.88774418986797,331.984469407796));
#30056=CARTESIAN_POINT('Ctrl Pts',(49.6798670922801,3.80073016960812,331.87852066476));
#30057=CARTESIAN_POINT('Ctrl Pts',(49.6721151187571,3.7137816301583,331.772651651514));
#30058=CARTESIAN_POINT('Ctrl Pts',(49.6643631452341,3.62233865618957,331.670335970566));
#30059=CARTESIAN_POINT('Ctrl Pts',(49.6566111717111,3.52672786607519,331.571972342418));
#30060=CARTESIAN_POINT('Ctrl Pts',(49.6488624811535,3.43115756718693,331.473650371324));
#30061=CARTESIAN_POINT('Ctrl Pts',(49.6411137905959,3.33142323463103,331.379277403864));
#30062=CARTESIAN_POINT('Ctrl Pts',(49.6333651000382,3.22789041915044,331.289217534743));
#30063=CARTESIAN_POINT('Ctrl Pts',(49.6256180216604,3.12437914453698,331.19917640333));
#30064=CARTESIAN_POINT('Ctrl Pts',(49.6178709432826,3.01707125370011,331.113446841685));
#30065=CARTESIAN_POINT('Ctrl Pts',(49.6101238649048,2.90636736276843,331.032354373796));
#30066=CARTESIAN_POINT('Ctrl Pts',(49.602376721599,2.79566254403151,330.951261226275));
#30067=CARTESIAN_POINT('Ctrl Pts',(49.5946295782931,2.68156198375639,330.874805481008));
#30068=CARTESIAN_POINT('Ctrl Pts',(49.5868824349873,2.56449709057508,330.803270590694));
#30069=CARTESIAN_POINT('Ctrl Pts',(49.5791335499592,2.44740587872018,330.731719617818));
#30070=CARTESIAN_POINT('Ctrl Pts',(49.5713846649311,2.32734934127482,330.665091905105));
#30071=CARTESIAN_POINT('Ctrl Pts',(49.563635779903,2.2047850510028,330.603625818771));
#30072=CARTESIAN_POINT('Ctrl Pts',(49.5558786701283,2.08209066972701,330.542094491699));
#30073=CARTESIAN_POINT('Ctrl Pts',(49.5481215603535,1.9568835684702,330.48573591053));
#30074=CARTESIAN_POINT('Ctrl Pts',(49.5403644505788,1.82964345236461,330.434741201233));
#30075=CARTESIAN_POINT('Ctrl Pts',(49.5326031956526,1.70233534320933,330.383719241993));
#30076=CARTESIAN_POINT('Ctrl Pts',(49.5248419407265,1.57299242290108,330.338066995978));
#30077=CARTESIAN_POINT('Ctrl Pts',(49.5170806858003,1.4421103159632,330.297925893917));
#30078=CARTESIAN_POINT('Ctrl Pts',(49.5093070153956,1.31101884030859,330.257720579175));
#30079=CARTESIAN_POINT('Ctrl Pts',(49.501533344991,1.17838363618827,330.223044124354));
#30080=CARTESIAN_POINT('Ctrl Pts',(49.4937596745863,1.04471216789936,330.193987146423));
#30081=CARTESIAN_POINT('Ctrl Pts',(49.4863478704093,0.91726313861926,330.166282777806));
#30082=CARTESIAN_POINT('Ctrl Pts',(49.4789360662322,0.78887243366812,330.143686536353));
#30083=CARTESIAN_POINT('Ctrl Pts',(49.4715242620551,0.659983012809761,330.126232926647));
#30084=CARTESIAN_POINT('Ctrl Pts',(49.4637491832767,0.524776337492697,330.107923863537));
#30085=CARTESIAN_POINT('Ctrl Pts',(49.4559741044982,0.388593544978953,330.09521643002));
#30086=CARTESIAN_POINT('Ctrl Pts',(49.4481990257198,0.251938440804253,330.088207039731));
#30087=CARTESIAN_POINT('Ctrl Pts',(49.4404335146707,0.115451499434481,330.081206274944));
#30088=CARTESIAN_POINT('Ctrl Pts',(49.4326680036217,-0.0215062105264285,
330.079889621736));
#30089=CARTESIAN_POINT('Ctrl Pts',(49.4249024925726,-0.158422675780561,
330.084302153478));
#30090=CARTESIAN_POINT('Ctrl Pts',(49.4171446810504,-0.295203387959936,
330.088710310183));
#30091=CARTESIAN_POINT('Ctrl Pts',(49.4093868695282,-0.431942548659525,
330.098836334805));
#30092=CARTESIAN_POINT('Ctrl Pts',(49.4016290580061,-0.568125386221159,
330.11467333661));
#30093=CARTESIAN_POINT('Ctrl Pts',(49.3938770844831,-0.704205741878459,
330.130498420569));
#30094=CARTESIAN_POINT('Ctrl Pts',(49.3861251109601,-0.839730221007358,
330.152025882396));
#30095=CARTESIAN_POINT('Ctrl Pts',(49.3783731374371,-0.974186779090219,
330.179196832275));
#30096=CARTESIAN_POINT('Ctrl Pts',(49.3706244468795,-1.10858639474154,330.206356275241));
#30097=CARTESIAN_POINT('Ctrl Pts',(49.3628757563218,-1.24191860653802,330.239154375414));
#30098=CARTESIAN_POINT('Ctrl Pts',(49.3551270657642,-1.37367941899319,330.277480765912));
#30099=CARTESIAN_POINT('Ctrl Pts',(49.3473799873864,-1.50541281751075,330.315799182284));
#30100=CARTESIAN_POINT('Ctrl Pts',(49.3396329090086,-1.63557509191617,330.359643492034));
#30101=CARTESIAN_POINT('Ctrl Pts',(49.3318858306307,-1.76367570576659,330.408852968224));
#30102=CARTESIAN_POINT('Ctrl Pts',(49.324138687325,-1.89177739322301,330.458062856836));
#30103=CARTESIAN_POINT('Ctrl Pts',(49.3163915440191,-2.01781702078277,330.512637861406));
#30104=CARTESIAN_POINT('Ctrl Pts',(49.3086444007133,-2.14132276705989,330.572368593732));
#30105=CARTESIAN_POINT('Ctrl Pts',(49.3008955156853,-2.26485628005096,330.632112754795));
#30106=CARTESIAN_POINT('Ctrl Pts',(49.2931466306572,-2.38585442636517,330.69701477998));
#30107=CARTESIAN_POINT('Ctrl Pts',(49.2853977456291,-2.50386913988776,330.766818880225));
#30108=CARTESIAN_POINT('Ctrl Pts',(49.2776406358544,-2.62200911544685,330.836697071264));
#30109=CARTESIAN_POINT('Ctrl Pts',(49.2698835260797,-2.73715899558075,330.911487531762));
#30110=CARTESIAN_POINT('Ctrl Pts',(49.2621264163049,-2.84889846241441,330.990890296668));
#30111=CARTESIAN_POINT('Ctrl Pts',(49.2543651613788,-2.96069763924648,331.070335491872));
#30112=CARTESIAN_POINT('Ctrl Pts',(49.2466039064526,-3.0690824627426,331.154397663125));
#30113=CARTESIAN_POINT('Ctrl Pts',(49.2388426515264,-3.1736657899163,331.242736565475));
#30114=CARTESIAN_POINT('Ctrl Pts',(49.2310689811218,-3.27841641632978,331.33121678128));
#30115=CARTESIAN_POINT('Ctrl Pts',(49.2232953107171,-3.37935310653415,331.423987134635));
#30116=CARTESIAN_POINT('Ctrl Pts',(49.2155216403125,-3.47612504073809,331.520669926027));
#30117=CARTESIAN_POINT('Ctrl Pts',(49.2081098361354,-3.56839221812225,331.612852110219));
#30118=CARTESIAN_POINT('Ctrl Pts',(49.2006980319584,-3.65687345713565,331.708590470285));
#30119=CARTESIAN_POINT('Ctrl Pts',(49.1932862277814,-3.74130003119369,331.80753118432));
#30120=CARTESIAN_POINT('Ctrl Pts',(49.1855629235076,-3.82927484875019,331.910630135843));
#30121=CARTESIAN_POINT('Ctrl Pts',(49.1778396192339,-3.91313527088013,332.017544756288));
#30122=CARTESIAN_POINT('Ctrl Pts',(49.1701163149601,-3.99252856049073,332.127910385074));
#30123=CARTESIAN_POINT('Ctrl Pts',(49.1624054455346,-4.07179402352995,332.238098320506));
#30124=CARTESIAN_POINT('Ctrl Pts',(49.1546945761091,-4.14660644630111,332.351725881446));
#30125=CARTESIAN_POINT('Ctrl Pts',(49.1469837066835,-4.21665188104645,332.468393795124));
#30126=CARTESIAN_POINT('Ctrl Pts',(49.1392800286901,-4.28663198891882,332.584952900141));
#30127=CARTESIAN_POINT('Ctrl Pts',(49.1315763506966,-4.35185374767205,332.704546381286));
#30128=CARTESIAN_POINT('Ctrl Pts',(49.1238726727032,-4.41204511106492,332.826744147499));
#30129=CARTESIAN_POINT('Ctrl Pts',(49.1161744546254,-4.47219381434558,332.948855307095));
#30130=CARTESIAN_POINT('Ctrl Pts',(49.1084762365477,-4.5273190398065,333.073566725879));
#30131=CARTESIAN_POINT('Ctrl Pts',(49.1007780184699,-4.57719374991476,333.200422149991));
#30132=CARTESIAN_POINT('Ctrl Pts',(49.0930835331751,-4.62704427631365,333.327216063276));
#30133=CARTESIAN_POINT('Ctrl Pts',(49.0853890478803,-4.67164920880391,333.456151544821));
#30134=CARTESIAN_POINT('Ctrl Pts',(49.0776945625855,-4.71082909366054,333.586751149719));
#30135=CARTESIAN_POINT('Ctrl Pts',(49.0700007301838,-4.75000565402211,333.717339672967));
#30136=CARTESIAN_POINT('Ctrl Pts',(49.0623068977822,-4.78375796038099,333.849591661466));
#30137=CARTESIAN_POINT('Ctrl Pts',(49.0546130653805,-4.81195608938995,333.983013443411));
#30138=CARTESIAN_POINT('Ctrl Pts',(49.0469196794052,-4.84015258223297,334.116427483701));
#30139=CARTESIAN_POINT('Ctrl Pts',(49.0392262934298,-4.86279546241927,334.25101079316));
#30140=CARTESIAN_POINT('Ctrl Pts',(49.0315329074544,-4.87980586329072,334.38625917596));
#30141=CARTESIAN_POINT('Ctrl Pts',(49.0238358959717,-4.89682428031193,334.521571294547));
#30142=CARTESIAN_POINT('Ctrl Pts',(49.0161388844889,-4.90820487232326,334.657548718119));
#30143=CARTESIAN_POINT('Ctrl Pts',(49.0084418730062,-4.91392062046323,334.793681803308));
#30144=CARTESIAN_POINT('Ctrl Pts',(49.0044733315008,-4.91686763227146,334.863871356752));
#30145=CARTESIAN_POINT('Ctrl Pts',(49.0005047899955,-4.91830956042976,334.934102250792));
#30146=CARTESIAN_POINT('Ctrl Pts',(48.9965362484901,-4.91824811618314,335.004304667347));
#30147=CARTESIAN_POINT('',(52.4965362484542,-4.91824882173218,334.996595586683));
#30148=CARTESIAN_POINT('Ctrl Pts',(52.4965362484542,-4.91824882173218,334.996595586683));
#30149=CARTESIAN_POINT('Ctrl Pts',(52.4888775572962,-4.91834206568241,335.131302188295));
#30150=CARTESIAN_POINT('Ctrl Pts',(52.4812188661381,-4.91289690048249,335.266224549053));
#30151=CARTESIAN_POINT('Ctrl Pts',(52.47356017498,-4.9018866689054,335.400861756354));
#30152=CARTESIAN_POINT('Ctrl Pts',(52.4659095597492,-4.8908880473839,335.535356991577));
#30153=CARTESIAN_POINT('Ctrl Pts',(52.4582589445185,-4.87433606304535,335.669567273004));
#30154=CARTESIAN_POINT('Ctrl Pts',(52.4506083292877,-4.85225607951328,335.802990660797));
#30155=CARTESIAN_POINT('Ctrl Pts',(52.4429638300524,-4.8301937469903,335.9363073883));
#30156=CARTESIAN_POINT('Ctrl Pts',(52.4353193308171,-4.8026122716787,336.068838077947));
#30157=CARTESIAN_POINT('Ctrl Pts',(52.4276748315818,-4.76958887882669,336.200085409241));
#30158=CARTESIAN_POINT('Ctrl Pts',(52.4200339012011,-4.73658090303234,336.331271467374));
#30159=CARTESIAN_POINT('Ctrl Pts',(52.4123929708203,-4.69813615873357,336.46117496852));
#30160=CARTESIAN_POINT('Ctrl Pts',(52.4047520404396,-4.65438298141709,336.589308693991));
#30161=CARTESIAN_POINT('Ctrl Pts',(52.3971128016806,-4.61063949059459,336.717414052001));
#30162=CARTESIAN_POINT('Ctrl Pts',(52.3894735629215,-4.56159003326485,336.843750032233));
#30163=CARTESIAN_POINT('Ctrl Pts',(52.3818343241625,-4.50741267909441,336.967845014944));
#30164=CARTESIAN_POINT('Ctrl Pts',(52.3741950142381,-4.45323482022019,337.091941153695));
#30165=CARTESIAN_POINT('Ctrl Pts',(52.3665557043138,-4.39392913095153,337.213795884254));
#30166=CARTESIAN_POINT('Ctrl Pts',(52.3589163943894,-4.3297214253522,337.332958516851));
#30167=CARTESIAN_POINT('Ctrl Pts',(52.3512752506671,-4.26549830684867,337.452149754148));
#30168=CARTESIAN_POINT('Ctrl Pts',(52.3436341069449,-4.19637102359047,337.568647254121));
#30169=CARTESIAN_POINT('Ctrl Pts',(52.3359929632226,-4.12261055905108,337.682026331135));
#30170=CARTESIAN_POINT('Ctrl Pts',(52.3283438794186,-4.04877344837884,337.795523222859));
#30171=CARTESIAN_POINT('Ctrl Pts',(52.3206947956146,-3.97029376465579,337.905894884365));
#30172=CARTESIAN_POINT('Ctrl Pts',(52.3130457118107,-3.88748507880771,338.012746724261));
#30173=CARTESIAN_POINT('Ctrl Pts',(52.305392237099,-3.8046288571621,338.119659901775));
#30174=CARTESIAN_POINT('Ctrl Pts',(52.2977387623873,-3.71743894559341,338.223048928115));
#30175=CARTESIAN_POINT('Ctrl Pts',(52.2900852876756,-3.62626726704912,338.322554554921));
#30176=CARTESIAN_POINT('Ctrl Pts',(52.282420522707,-3.53496109382011,338.422206970491));
#30177=CARTESIAN_POINT('Ctrl Pts',(52.2747557577385,-3.43966171024998,338.517964264827));
#30178=CARTESIAN_POINT('Ctrl Pts',(52.2670909927699,-3.34075603402147,338.609505808784));
#30179=CARTESIAN_POINT('Ctrl Pts',(52.2626955301115,-3.28403724246679,338.662001539548));
#30180=CARTESIAN_POINT('Ctrl Pts',(52.2583000674531,-3.22613307481586,338.713111638871));
#30181=CARTESIAN_POINT('Ctrl Pts',(52.2539046047947,-3.16712081781979,338.762782054256));
#30182=CARTESIAN_POINT('Ctrl Pts',(52.2461295260163,-3.0627347764188,338.850643429176));
#30183=CARTESIAN_POINT('Ctrl Pts',(52.2383544472378,-2.95452487634904,338.934296578371));
#30184=CARTESIAN_POINT('Ctrl Pts',(52.2305793684594,-2.84286498459752,339.013390305197));
#30185=CARTESIAN_POINT('Ctrl Pts',(52.2228138574103,-2.73134249745118,339.092386702157));
#30186=CARTESIAN_POINT('Ctrl Pts',(52.2150483463614,-2.61637878173231,339.166834616576));
#30187=CARTESIAN_POINT('Ctrl Pts',(52.2072828353123,-2.49838212722402,339.236421816683));
#30188=CARTESIAN_POINT('Ctrl Pts',(52.1995250237901,-2.38050246674245,339.305940020878));
#30189=CARTESIAN_POINT('Ctrl Pts',(52.1917672122679,-2.25959618642276,339.370606904387));
#30190=CARTESIAN_POINT('Ctrl Pts',(52.1840094007457,-2.13610173055205,339.430152645139));
#30191=CARTESIAN_POINT('Ctrl Pts',(52.1762574272226,-2.01270020817519,339.489653575833));
#30192=CARTESIAN_POINT('Ctrl Pts',(52.1685054536996,-1.8867147376829,339.544040865534));
#30193=CARTESIAN_POINT('Ctrl Pts',(52.1607534801766,-1.75860930377084,339.5930900687));
#30194=CARTESIAN_POINT('Ctrl Pts',(52.1530047896189,-1.63055812258654,339.6421184995));
#30195=CARTESIAN_POINT('Ctrl Pts',(52.1452560990614,-1.50038912792764,339.685813200631));
#30196=CARTESIAN_POINT('Ctrl Pts',(52.1375074085038,-1.36858707073141,339.723997511888));
#30197=CARTESIAN_POINT('Ctrl Pts',(52.1297603301259,-1.23681243605401,339.762173878581));
#30198=CARTESIAN_POINT('Ctrl Pts',(52.122013251748,-1.10340578987091,339.794842027137));
#30199=CARTESIAN_POINT('Ctrl Pts',(52.1142661733702,-0.968867482173869,
339.821875036175));
#30200=CARTESIAN_POINT('Ctrl Pts',(52.1065190300644,-0.834328046916041,
339.848908271776));
#30201=CARTESIAN_POINT('Ctrl Pts',(52.0987718867586,-0.698657314441851,
339.87030619666));
#30202=CARTESIAN_POINT('Ctrl Pts',(52.0910247434527,-0.562365885146263,
339.885993007949));
#30203=CARTESIAN_POINT('Ctrl Pts',(52.0832758584246,-0.426043814644006,
339.901683345966));
#30204=CARTESIAN_POINT('Ctrl Pts',(52.0755269733965,-0.289101157874568,
339.911659970726));
#30205=CARTESIAN_POINT('Ctrl Pts',(52.0677780883684,-0.152053298517322,
339.915898987663));
#30206=CARTESIAN_POINT('Ctrl Pts',(52.0600209785937,-0.0148599751461849,
339.920142503937));
#30207=CARTESIAN_POINT('Ctrl Pts',(52.0522638688189,0.122438382565781,339.918636235025));
#30208=CARTESIAN_POINT('Ctrl Pts',(52.0445067590442,0.25932617128518,339.911408453732));
#30209=CARTESIAN_POINT('Ctrl Pts',(52.036745504118,0.396287108462141,339.904176810143));
#30210=CARTESIAN_POINT('Ctrl Pts',(52.0289842491918,0.53283665055394,339.891217598954));
#30211=CARTESIAN_POINT('Ctrl Pts',(52.0212229942656,0.668465643909878,339.872610875641));
#30212=CARTESIAN_POINT('Ctrl Pts',(52.013449323861,0.804311599453707,339.853974387634));
#30213=CARTESIAN_POINT('Ctrl Pts',(52.0056756534563,0.939233678728462,339.829672403864));
#30214=CARTESIAN_POINT('Ctrl Pts',(51.9979019830517,1.07273334956113,339.799836062121));
#30215=CARTESIAN_POINT('Ctrl Pts',(51.9904901788746,1.20001857859784,339.771388609265));
#30216=CARTESIAN_POINT('Ctrl Pts',(51.9830783746975,1.32601056710423,339.73791052572));
#30217=CARTESIAN_POINT('Ctrl Pts',(51.9756665705205,1.45029290098457,339.69955674121));
#30218=CARTESIAN_POINT('Ctrl Pts',(51.967891491742,1.5806666822669,339.659323123471));
#30219=CARTESIAN_POINT('Ctrl Pts',(51.9601164129636,1.70957098609738,339.613596628992));
#30220=CARTESIAN_POINT('Ctrl Pts',(51.9523413341851,1.83650816284588,339.562501597841));
#30221=CARTESIAN_POINT('Ctrl Pts',(51.9445758231361,1.96328913531692,339.511469442379));
#30222=CARTESIAN_POINT('Ctrl Pts',(51.9368103120871,2.08810743802025,339.4550820395));
#30223=CARTESIAN_POINT('Ctrl Pts',(51.9290448010381,2.21047955956878,339.393513762267));
#30224=CARTESIAN_POINT('Ctrl Pts',(51.9212869895159,2.33273034880319,339.332006530159));
#30225=CARTESIAN_POINT('Ctrl Pts',(51.9135291779937,2.45253943663542,339.265328820867));
#30226=CARTESIAN_POINT('Ctrl Pts',(51.9057713664715,2.56944265656888,339.193703315341));
#30227=CARTESIAN_POINT('Ctrl Pts',(51.8980193929485,2.68625790312165,339.12213171028));
#30228=CARTESIAN_POINT('Ctrl Pts',(51.8902674194254,2.80017130246058,339.04561992356));
#30229=CARTESIAN_POINT('Ctrl Pts',(51.8825154459024,2.91074302479976,338.96443666945));
#30230=CARTESIAN_POINT('Ctrl Pts',(51.8747667553448,3.02126791994889,338.883287796496));
#30231=CARTESIAN_POINT('Ctrl Pts',(51.8670180647872,3.12845363842076,338.797471621837));
#30232=CARTESIAN_POINT('Ctrl Pts',(51.8592693742296,3.23188929633324,338.707300181904));
#30233=CARTESIAN_POINT('Ctrl Pts',(51.8515222958517,3.33530343359317,338.617147502892));
#30234=CARTESIAN_POINT('Ctrl Pts',(51.8437752174739,3.43496876777921,338.522641617692));
#30235=CARTESIAN_POINT('Ctrl Pts',(51.8360281390961,3.53050779990477,338.424134596845));
#30236=CARTESIAN_POINT('Ctrl Pts',(51.8282809957903,3.62604763273911,338.325626750415));
#30237=CARTESIAN_POINT('Ctrl Pts',(51.8205338524845,3.71746082240527,338.223117982037));
#30238=CARTESIAN_POINT('Ctrl Pts',(51.8127867091787,3.8044073094734,338.11699664519));
#30239=CARTESIAN_POINT('Ctrl Pts',(51.8050378241506,3.89137334395804,338.010851450013));
#30240=CARTESIAN_POINT('Ctrl Pts',(51.7972889391225,3.97387042990715,337.901092372509));
#30241=CARTESIAN_POINT('Ctrl Pts',(51.7895400540944,4.05159957018778,337.788139879087));
#30242=CARTESIAN_POINT('Ctrl Pts',(51.7817829443197,4.12941121298095,337.675067496721));
#30243=CARTESIAN_POINT('Ctrl Pts',(51.774025834545,4.2024445788538,337.558795250051));
#30244=CARTESIAN_POINT('Ctrl Pts',(51.7662687247703,4.27044442046223,337.439772020957));
#30245=CARTESIAN_POINT('Ctrl Pts',(51.7585074698441,4.33848059901175,337.320685189654));
#30246=CARTESIAN_POINT('Ctrl Pts',(51.7507462149179,4.40147771428681,337.198844793779));
#30247=CARTESIAN_POINT('Ctrl Pts',(51.7429849599917,4.45922755439041,337.07472231411));
#30248=CARTESIAN_POINT('Ctrl Pts',(51.7352112895871,4.51706977541754,336.950401278925));
#30249=CARTESIAN_POINT('Ctrl Pts',(51.7274376191824,4.56964779772785,336.823791226161));
#30250=CARTESIAN_POINT('Ctrl Pts',(51.7196639487778,4.61680211352313,336.695382348342));
#30251=CARTESIAN_POINT('Ctrl Pts',(51.7122521446007,4.66176138457331,336.572950934679));
#30252=CARTESIAN_POINT('Ctrl Pts',(51.7048403404237,4.70179044429626,336.448884671644));
#30253=CARTESIAN_POINT('Ctrl Pts',(51.6974285362466,4.73679423084125,336.323617572099));
#30254=CARTESIAN_POINT('Ctrl Pts',(51.6896534574682,4.77351365723589,336.192210758853));
#30255=CARTESIAN_POINT('Ctrl Pts',(51.6818783786898,4.80481878782615,336.059067149761));
#30256=CARTESIAN_POINT('Ctrl Pts',(51.6741032999113,4.83054487605908,335.924672516559));
#30257=CARTESIAN_POINT('Ctrl Pts',(51.6663377888623,4.85623930670258,335.79044326451));
#30258=CARTESIAN_POINT('Ctrl Pts',(51.6585722778133,4.87636828231503,335.654966431679));
#30259=CARTESIAN_POINT('Ctrl Pts',(51.6508067667643,4.89081678116865,335.518742976376));
#30260=CARTESIAN_POINT('Ctrl Pts',(51.6430489552421,4.90525095429364,335.382654587025));
#30261=CARTESIAN_POINT('Ctrl Pts',(51.6352911437199,4.91401581811348,335.245821434588));
#30262=CARTESIAN_POINT('Ctrl Pts',(51.6275333321977,4.91704744266493,335.108754352015));
#30263=CARTESIAN_POINT('Ctrl Pts',(51.6197813586747,4.92007678582278,334.971790416768));
#30264=CARTESIAN_POINT('Ctrl Pts',(51.6120293851516,4.91738146879444,334.834593290988));
#30265=CARTESIAN_POINT('Ctrl Pts',(51.6042774116286,4.90894944200643,334.697678253636));
#30266=CARTESIAN_POINT('Ctrl Pts',(51.596528721071,4.9005209861868,334.560821199883));
#30267=CARTESIAN_POINT('Ctrl Pts',(51.5887800305134,4.88636067668862,334.424246386274));
#30268=CARTESIAN_POINT('Ctrl Pts',(51.5810313399558,4.86650855875888,334.288468194649));
#30269=CARTESIAN_POINT('Ctrl Pts',(51.573284261578,4.84666057122808,334.15271825281));
#30270=CARTESIAN_POINT('Ctrl Pts',(51.5655371832001,4.82112318729248,334.017764989798));
#30271=CARTESIAN_POINT('Ctrl Pts',(51.5577901048223,4.78998818421876,333.884116378136));
#30272=CARTESIAN_POINT('Ctrl Pts',(51.5500429615165,4.75885292020376,333.75046664637));
#30273=CARTESIAN_POINT('Ctrl Pts',(51.5422958182107,4.72212003216232,333.618121968443));
#30274=CARTESIAN_POINT('Ctrl Pts',(51.5345486749049,4.6799320691492,333.487578467937));
#30275=CARTESIAN_POINT('Ctrl Pts',(51.5267997898768,4.63773462138643,333.35700561848));
#30276=CARTESIAN_POINT('Ctrl Pts',(51.5190509048487,4.59007977839495,333.228235124096));
#30277=CARTESIAN_POINT('Ctrl Pts',(51.5113020198206,4.53715931484396,333.101745956352));
#30278=CARTESIAN_POINT('Ctrl Pts',(51.5035449100459,4.48418268096593,332.975122531699));
#30279=CARTESIAN_POINT('Ctrl Pts',(51.4957878002712,4.42592941310896,332.850785631865));
#30280=CARTESIAN_POINT('Ctrl Pts',(51.4880306904965,4.36263885663847,332.729192815528));
#30281=CARTESIAN_POINT('Ctrl Pts',(51.4802694355703,4.29931447971815,332.607535023879));
#30282=CARTESIAN_POINT('Ctrl Pts',(51.4725081806441,4.23094764532456,332.48862457625));
#30283=CARTESIAN_POINT('Ctrl Pts',(51.4647469257179,4.15782215629907,332.372891707773));
#30284=CARTESIAN_POINT('Ctrl Pts',(51.4569732553133,4.08457969032283,332.256973704423));
#30285=CARTESIAN_POINT('Ctrl Pts',(51.4491995849086,4.00656358064499,332.144243759326));
#30286=CARTESIAN_POINT('Ctrl Pts',(51.441425914504,3.92409972179423,332.035101277292));
#30287=CARTESIAN_POINT('Ctrl Pts',(51.4340141103269,3.84547457541285,331.931039404056));
#30288=CARTESIAN_POINT('Ctrl Pts',(51.4266023061498,3.76280662907251,331.830238739903));
#30289=CARTESIAN_POINT('Ctrl Pts',(51.4191905019727,3.6764094100248,331.733014093636));
#30290=CARTESIAN_POINT('Ctrl Pts',(51.4114154231943,3.58577760590738,331.631024177838));
#30291=CARTESIAN_POINT('Ctrl Pts',(51.4036403444159,3.4907553069779,331.532647379));
#30292=CARTESIAN_POINT('Ctrl Pts',(51.3958652656375,3.39166185524052,331.438285114975));
#30293=CARTESIAN_POINT('Ctrl Pts',(51.3880997545885,3.29269034430423,331.344038969724));
#30294=CARTESIAN_POINT('Ctrl Pts',(51.3803342435395,3.18965792900957,331.253797796795));
#30295=CARTESIAN_POINT('Ctrl Pts',(51.3725687324905,3.08292363102994,331.167929417699));
#30296=CARTESIAN_POINT('Ctrl Pts',(51.3648109209683,2.97629516041743,331.082146177351));
#30297=CARTESIAN_POINT('Ctrl Pts',(51.3570531094461,2.86597241406727,331.000727346107));
#30298=CARTESIAN_POINT('Ctrl Pts',(51.349295297924,2.75235036613324,330.924003125057));
#30299=CARTESIAN_POINT('Ctrl Pts',(51.341543324401,2.6388138223936,330.847336641416));
#30300=CARTESIAN_POINT('Ctrl Pts',(51.333791350878,2.52198324165249,330.775357953879));
#30301=CARTESIAN_POINT('Ctrl Pts',(51.326039377355,2.40228541226457,330.7083560422));
#30302=CARTESIAN_POINT('Ctrl Pts',(51.3182906867974,2.28263827497823,330.64138250587));
#30303=CARTESIAN_POINT('Ctrl Pts',(51.3105419962398,2.16012664453082,330.579381743919));
#30304=CARTESIAN_POINT('Ctrl Pts',(51.3027933056822,2.03520474636636,330.522598442973));
#30305=CARTESIAN_POINT('Ctrl Pts',(51.2950462273044,1.91030883924635,330.465826956267));
#30306=CARTESIAN_POINT('Ctrl Pts',(51.2872991489266,1.78300401749595,330.414270933002));
#30307=CARTESIAN_POINT('Ctrl Pts',(51.2795520705488,1.65376711199213,330.368128088797));
#30308=CARTESIAN_POINT('Ctrl Pts',(51.2718049272429,1.52452912335803,330.32198485787));
#30309=CARTESIAN_POINT('Ctrl Pts',(51.2640577839371,1.39335938678749,330.281255027923));
#30310=CARTESIAN_POINT('Ctrl Pts',(51.2563106406313,1.26075224465636,330.246087207353));
#30311=CARTESIAN_POINT('Ctrl Pts',(51.2485617556032,1.12811528962479,330.21091148031));
#30312=CARTESIAN_POINT('Ctrl Pts',(51.2408128705751,0.994040663721647,330.181300351092));
#30313=CARTESIAN_POINT('Ctrl Pts',(51.233063985547,0.859034924634935,330.157351751288));
#30314=CARTESIAN_POINT('Ctrl Pts',(51.2253068757723,0.723885889061702,330.133377732192));
#30315=CARTESIAN_POINT('Ctrl Pts',(51.2175497659976,0.587804151570398,330.115078316962));
#30316=CARTESIAN_POINT('Ctrl Pts',(51.2097926562228,0.451304006526837,330.102499846228));
#30317=CARTESIAN_POINT('Ctrl Pts',(51.2020314012967,0.314730920170378,330.089914653963));
#30318=CARTESIAN_POINT('Ctrl Pts',(51.1942701463705,0.177739370938527,330.083056517255));
#30319=CARTESIAN_POINT('Ctrl Pts',(51.1865088914444,0.0408447347324409,
330.081919605156));
#30320=CARTESIAN_POINT('Ctrl Pts',(51.1787352210397,-0.0962688882778101,
330.080780874369));
#30321=CARTESIAN_POINT('Ctrl Pts',(51.1709615506351,-0.233284897608335,
330.085381643663));
#30322=CARTESIAN_POINT('Ctrl Pts',(51.1631878802304,-0.369691065002353,
330.095664002237));
#30323=CARTESIAN_POINT('Ctrl Pts',(51.1557760760532,-0.499747492488417,
330.105467714545));
#30324=CARTESIAN_POINT('Ctrl Pts',(51.148364271876,-0.629249290714439,330.120435930953));
#30325=CARTESIAN_POINT('Ctrl Pts',(51.1409524676988,-0.757762062657612,
330.14047536081));
#30326=CARTESIAN_POINT('Ctrl Pts',(51.1331773889204,-0.892573628372065,
330.161496982818));
#30327=CARTESIAN_POINT('Ctrl Pts',(51.125402310142,-1.02672279562088,330.18816593049));
#30328=CARTESIAN_POINT('Ctrl Pts',(51.1176272313635,-1.15969918928645,330.220430892552));
#30329=CARTESIAN_POINT('Ctrl Pts',(51.1098617203145,-1.29251194703411,330.252656150525));
#30330=CARTESIAN_POINT('Ctrl Pts',(51.1020962092655,-1.42415442647661,330.290463629938));
#30331=CARTESIAN_POINT('Ctrl Pts',(51.0943306982164,-1.55412303142994,330.33375047113));
#30332=CARTESIAN_POINT('Ctrl Pts',(51.0865728866942,-1.68396277213262,330.376994393293));
#30333=CARTESIAN_POINT('Ctrl Pts',(51.078815075172,-1.81213157268847,330.425706742934));
#30334=CARTESIAN_POINT('Ctrl Pts',(51.0710572636498,-1.93813801677779,330.479734068617));
#30335=CARTESIAN_POINT('Ctrl Pts',(51.0633052901268,-2.06404963702264,330.533720737024));
#30336=CARTESIAN_POINT('Ctrl Pts',(51.0555533166038,-2.1878017819479,330.593014266879));
#30337=CARTESIAN_POINT('Ctrl Pts',(51.0478013430807,-2.30892048264449,330.657412146274));
#30338=CARTESIAN_POINT('Ctrl Pts',(51.0400526525231,-2.42998788949892,330.72178275313));
#30339=CARTESIAN_POINT('Ctrl Pts',(51.0323039619654,-2.54842372590289,330.791253226949));
#30340=CARTESIAN_POINT('Ctrl Pts',(51.0245552714078,-2.66377642220092,330.865574013841));
#30341=CARTESIAN_POINT('Ctrl Pts',(51.0168081930299,-2.77910511840727,330.939879337672));
#30342=CARTESIAN_POINT('Ctrl Pts',(51.0090611146521,-2.89135162206878,331.019032755739));
#30343=CARTESIAN_POINT('Ctrl Pts',(51.0013140362742,-3.00009162935601,331.102740286051));
#30344=CARTESIAN_POINT('Ctrl Pts',(50.9935668929684,-3.10883254798894,331.186448517913));
#30345=CARTESIAN_POINT('Ctrl Pts',(50.9858197496626,-3.21406660189955,331.274710699717));
#30346=CARTESIAN_POINT('Ctrl Pts',(50.9780726063568,-3.31540130609275,331.367191548945));
#30347=CARTESIAN_POINT('Ctrl Pts',(50.9703237213287,-3.4167587924785,331.45969318983));
#30348=CARTESIAN_POINT('Ctrl Pts',(50.9625748363006,-3.51421489603983,331.556415122003));
#30349=CARTESIAN_POINT('Ctrl Pts',(50.9548259512726,-3.60741313658341,331.656984366697));
#30350=CARTESIAN_POINT('Ctrl Pts',(50.9470688414978,-3.70071029870273,331.757660356628));
#30351=CARTESIAN_POINT('Ctrl Pts',(50.9393117317231,-3.78974030389571,331.862191529259));
#30352=CARTESIAN_POINT('Ctrl Pts',(50.9315546219484,-3.87418586914465,331.970170481063));
#30353=CARTESIAN_POINT('Ctrl Pts',(50.9237933670222,-3.95867655940367,332.078207133367));
#30354=CARTESIAN_POINT('Ctrl Pts',(50.916032112096,-4.03857770073597,332.18969491841));
#30355=CARTESIAN_POINT('Ctrl Pts',(50.9082708571698,-4.11361529703815,332.304197290143));
#30356=CARTESIAN_POINT('Ctrl Pts',(50.9004971867652,-4.18877292903972,332.418882828354));
#30357=CARTESIAN_POINT('Ctrl Pts',(50.8927235163605,-4.25905126861334,332.536592253965));
#30358=CARTESIAN_POINT('Ctrl Pts',(50.8849498459559,-4.3242218180849,332.656863484451));
#30359=CARTESIAN_POINT('Ctrl Pts',(50.8775380417789,-4.38635866279863,332.771536060221));
#30360=CARTESIAN_POINT('Ctrl Pts',(50.8701262376019,-4.44385242411905,332.88853704592));
#30361=CARTESIAN_POINT('Ctrl Pts',(50.8627144334249,-4.49654647498829,333.007450662902));
#30362=CARTESIAN_POINT('Ctrl Pts',(50.8541643290833,-4.55733324462683,333.144626957438));
#30363=CARTESIAN_POINT('Ctrl Pts',(50.8456142247417,-4.61189867345044,333.28472172135));
#30364=CARTESIAN_POINT('Ctrl Pts',(50.8370641204001,-4.65998033764655,333.42717886737));
#30365=CARTESIAN_POINT('Ctrl Pts',(50.8285467284448,-4.70787804315518,333.569090977564));
#30366=CARTESIAN_POINT('Ctrl Pts',(50.8200293364895,-4.74934137372882,333.713347197521));
#30367=CARTESIAN_POINT('Ctrl Pts',(50.8115119445342,-4.7841566456173,333.859373745394));
#30368=CARTESIAN_POINT('Ctrl Pts',(50.8030154818032,-4.81888636823912,334.005041471883));
#30369=CARTESIAN_POINT('Ctrl Pts',(50.7945190190723,-4.84700053829952,334.152470602505));
#30370=CARTESIAN_POINT('Ctrl Pts',(50.7860225563413,-4.86833456063157,334.301071056358));
#30371=CARTESIAN_POINT('Ctrl Pts',(50.7775592787733,-4.88958525734558,334.449091112176));
#30372=CARTESIAN_POINT('Ctrl Pts',(50.7690960012053,-4.90410856744097,334.598273112415));
#30373=CARTESIAN_POINT('Ctrl Pts',(50.7606327236373,-4.91179067866555,334.748017080987));
#30374=CARTESIAN_POINT('Ctrl Pts',(50.7559338986031,-4.91605579891569,334.831155168164));
#30375=CARTESIAN_POINT('Ctrl Pts',(50.7512350735689,-4.91821300605794,334.914466203605));
#30376=CARTESIAN_POINT('Ctrl Pts',(50.7465362485347,-4.9182495281824,334.997845694185));
#30377=CARTESIAN_POINT('',(54.2465362485459,-4.9182483994059,335.00396790137));
#30378=CARTESIAN_POINT('Ctrl Pts',(54.24653624849,-4.91824839940511,335.003967902354));
#30379=CARTESIAN_POINT('Ctrl Pts',(54.2339556148914,-4.91806968276805,335.225488679793));
#30380=CARTESIAN_POINT('Ctrl Pts',(54.2213749812928,-4.90292221337486,335.446423007763));
#30381=CARTESIAN_POINT('Ctrl Pts',(54.2087943476942,-4.87305733668216,335.665203168895));
#30382=CARTESIAN_POINT('Ctrl Pts',(54.2063865133669,-4.86734143416276,335.707075971086));
#30383=CARTESIAN_POINT('Ctrl Pts',(54.2039786790395,-4.86108652521291,335.748869975681));
#30384=CARTESIAN_POINT('Ctrl Pts',(54.2015708447122,-4.85429452218873,335.790574319307));
#30385=CARTESIAN_POINT('Ctrl Pts',(54.1937957659337,-4.83236263178532,335.925240792587));
#30386=CARTESIAN_POINT('Ctrl Pts',(54.1860206871553,-4.80478801956478,336.059206730811));
#30387=CARTESIAN_POINT('Ctrl Pts',(54.1782456083769,-4.77162544357483,336.191962117154));
#30388=CARTESIAN_POINT('Ctrl Pts',(54.1704800973278,-4.73850367624587,336.324554139541));
#30389=CARTESIAN_POINT('Ctrl Pts',(54.1627145862788,-4.69980772092743,336.45593819845));
#30390=CARTESIAN_POINT('Ctrl Pts',(54.1549490752298,-4.65564383708228,336.585611404077));
#30391=CARTESIAN_POINT('Ctrl Pts',(54.1471912637076,-4.61152374185654,336.715156038343));
#30392=CARTESIAN_POINT('Ctrl Pts',(54.1394334521854,-4.56194663233361,336.842992827472));
#30393=CARTESIAN_POINT('Ctrl Pts',(54.1316756406632,-4.50706927631419,336.968631403032));
#30394=CARTESIAN_POINT('Ctrl Pts',(54.1239236671402,-4.4522332172455,337.09417543158));
#30395=CARTESIAN_POINT('Ctrl Pts',(54.1161716936172,-4.39210500662631,337.217524182461));
#30396=CARTESIAN_POINT('Ctrl Pts',(54.1084197200942,-4.32689035373806,337.338205065692));
#30397=CARTESIAN_POINT('Ctrl Pts',(54.1006710295365,-4.26170331929394,337.458834840498));
#30398=CARTESIAN_POINT('Ctrl Pts',(54.0929223389789,-4.19143431239677,337.576798651674));
#30399=CARTESIAN_POINT('Ctrl Pts',(54.0851736484213,-4.11633593191898,337.691646625784));
#30400=CARTESIAN_POINT('Ctrl Pts',(54.0774265700435,-4.04125317628654,337.806470704813));
#30401=CARTESIAN_POINT('Ctrl Pts',(54.0696794916656,-3.96134325945718,337.918179909305));
#30402=CARTESIAN_POINT('Ctrl Pts',(54.0619324132877,-3.87690302318793,338.02635193117));
#30403=CARTESIAN_POINT('Ctrl Pts',(54.0541852699819,-3.79246207922818,338.134524859621));
#30404=CARTESIAN_POINT('Ctrl Pts',(54.0464381266761,-3.70349098061472,338.239160238203));
#30405=CARTESIAN_POINT('Ctrl Pts',(54.0386909833703,-3.61032765373224,338.339867855948));
#30406=CARTESIAN_POINT('Ctrl Pts',(54.0309420983422,-3.51714338175602,338.440598114904));
#30407=CARTESIAN_POINT('Ctrl Pts',(54.0231932133141,-3.41976527141893,338.537398568993));
#30408=CARTESIAN_POINT('Ctrl Pts',(54.015444328286,-3.31856870125198,338.629915265894));
#30409=CARTESIAN_POINT('Ctrl Pts',(54.0076872185113,-3.21726471999983,338.722530160973));
#30410=CARTESIAN_POINT('Ctrl Pts',(53.9999301087365,-3.11213447170504,338.810851951998));
#30411=CARTESIAN_POINT('Ctrl Pts',(53.9921729989618,-3.00358749407249,338.894566115494));
#30412=CARTESIAN_POINT('Ctrl Pts',(53.9844117440357,-2.89498251240583,338.978325013161));
#30413=CARTESIAN_POINT('Ctrl Pts',(53.9766504891095,-2.78295748242483,339.057471151778));
#30414=CARTESIAN_POINT('Ctrl Pts',(53.9688892341833,-2.66795079125739,339.131733490671));
#30415=CARTESIAN_POINT('Ctrl Pts',(53.9611155637787,-2.55276012686466,339.206114625104));
#30416=CARTESIAN_POINT('Ctrl Pts',(53.953341893374,-2.43457860717126,339.275596149943));
#30417=CARTESIAN_POINT('Ctrl Pts',(53.9455682229694,-2.31386984782282,339.339952694424));
#30418=CARTESIAN_POINT('Ctrl Pts',(53.9381564187923,-2.19878011026379,339.401313426276));
#30419=CARTESIAN_POINT('Ctrl Pts',(53.9307446146153,-2.08139338324387,339.458015450623));
#30420=CARTESIAN_POINT('Ctrl Pts',(53.9233328104383,-1.96212649404924,339.509904952862));
#30421=CARTESIAN_POINT('Ctrl Pts',(53.9155577316598,-1.83701397933638,339.564337714178));
#30422=CARTESIAN_POINT('Ctrl Pts',(53.9077826528814,-1.70943695894224,339.61364629062));
#30423=CARTESIAN_POINT('Ctrl Pts',(53.900007574103,-1.57985394961869,339.65760073003));
#30424=CARTESIAN_POINT('Ctrl Pts',(53.892242063054,-1.45043040043768,339.701501080704));
#30425=CARTESIAN_POINT('Ctrl Pts',(53.884476552005,-1.31900614054945,339.740060279425));
#30426=CARTESIAN_POINT('Ctrl Pts',(53.8767110409559,-1.18606156380943,339.773095539517));
#30427=CARTESIAN_POINT('Ctrl Pts',(53.8689532294337,-1.0532488020043,339.806098045051));
#30428=CARTESIAN_POINT('Ctrl Pts',(53.8611954179115,-0.918919100050427,
339.833587417843));
#30429=CARTESIAN_POINT('Ctrl Pts',(53.8534376063893,-0.783569655275992,
339.855430120785));
#30430=CARTESIAN_POINT('Ctrl Pts',(53.8456856328663,-0.648322065251018,
339.877256386401));
#30431=CARTESIAN_POINT('Ctrl Pts',(53.8379336593433,-0.512056644183368,
339.893444378163));
#30432=CARTESIAN_POINT('Ctrl Pts',(53.8301816858203,-0.375282124166118,
339.90391133584));
#30433=CARTESIAN_POINT('Ctrl Pts',(53.8224329952626,-0.238565528239298,
339.914373860754));
#30434=CARTESIAN_POINT('Ctrl Pts',(53.814684304705,-0.101340651107091,339.91912014072));
#30435=CARTESIAN_POINT('Ctrl Pts',(53.8069356141474,0.0358775033162497,
339.918119139189));
#30436=CARTESIAN_POINT('Ctrl Pts',(53.7991885357696,0.173067108356401,339.917118345924));
#30437=CARTESIAN_POINT('Ctrl Pts',(53.7914414573917,0.310249602851338,339.910372652482));
#30438=CARTESIAN_POINT('Ctrl Pts',(53.7836943790139,0.446909220811845,339.897903144291));
#30439=CARTESIAN_POINT('Ctrl Pts',(53.7759472357081,0.583569984111577,339.885433531593));
#30440=CARTESIAN_POINT('Ctrl Pts',(53.7682000924023,0.719707472878996,339.867240043981));
#30441=CARTESIAN_POINT('Ctrl Pts',(53.7604529490965,0.854810679030702,339.843395685417));
#30442=CARTESIAN_POINT('Ctrl Pts',(53.7527040640684,0.989944259251474,339.819545966135));
#30443=CARTESIAN_POINT('Ctrl Pts',(53.7449551790403,1.12404270930034,339.790042915798));
#30444=CARTESIAN_POINT('Ctrl Pts',(53.7372062940122,1.25660524425672,339.755010654311));
#30445=CARTESIAN_POINT('Ctrl Pts',(53.7294491842374,1.38930848245733,339.719941209219));
#30446=CARTESIAN_POINT('Ctrl Pts',(53.7216920744627,1.52047217051797,339.679330929599));
#30447=CARTESIAN_POINT('Ctrl Pts',(53.713934964688,1.64961019458591,339.633353997745));
#30448=CARTESIAN_POINT('Ctrl Pts',(53.7061737097618,1.77881722588479,339.587352497288));
#30449=CARTESIAN_POINT('Ctrl Pts',(53.6984124548357,1.90599607407346,339.535978776638));
#30450=CARTESIAN_POINT('Ctrl Pts',(53.6906511999095,2.03068157883941,339.479454809222));
#30451=CARTESIAN_POINT('Ctrl Pts',(53.6828775295048,2.15556653977817,339.42284042188));
#30452=CARTESIAN_POINT('Ctrl Pts',(53.6751038591001,2.27794983789881,339.361059500617));
#30453=CARTESIAN_POINT('Ctrl Pts',(53.6673301886955,2.39739106509028,339.294379948668));
#30454=CARTESIAN_POINT('Ctrl Pts',(53.6599183845184,2.51127227442001,339.230804345906));
#30455=CARTESIAN_POINT('Ctrl Pts',(53.6525065803413,2.62247891001836,339.162776061754));
#30456=CARTESIAN_POINT('Ctrl Pts',(53.6450947761642,2.73065605674223,339.090562377263));
#30457=CARTESIAN_POINT('Ctrl Pts',(53.6373196973858,2.84413528767021,339.014809284981));
#30458=CARTESIAN_POINT('Ctrl Pts',(53.6295446186073,2.95463916765595,338.934210746834));
#30459=CARTESIAN_POINT('Ctrl Pts',(53.6217695398289,3.06172619529895,338.849027899031));
#30460=CARTESIAN_POINT('Ctrl Pts',(53.6140040287799,3.16868144553693,338.763949874146));
#30461=CARTESIAN_POINT('Ctrl Pts',(53.6062385177309,3.27222790651429,338.674299005147));
#30462=CARTESIAN_POINT('Ctrl Pts',(53.5984730066818,3.37195190033349,338.580380349116));
#30463=CARTESIAN_POINT('Ctrl Pts',(53.5907151951596,3.47157701752247,338.486554813706));
#30464=CARTESIAN_POINT('Ctrl Pts',(53.5829573836375,3.56738692712724,338.388470178493));
#30465=CARTESIAN_POINT('Ctrl Pts',(53.5751995721153,3.6590002729416,338.286472282724));
#30466=CARTESIAN_POINT('Ctrl Pts',(53.5674475985922,3.75054467680788,338.184551143607));
#30467=CARTESIAN_POINT('Ctrl Pts',(53.5596956250692,3.8378985426843,338.078722895145));
#30468=CARTESIAN_POINT('Ctrl Pts',(53.5519436515462,3.92071697159911,337.969370554699));
#30469=CARTESIAN_POINT('Ctrl Pts',(53.5441949609886,4.00350032686016,337.860064525034));
#30470=CARTESIAN_POINT('Ctrl Pts',(53.536446270431,4.08175182991898,337.747237682721));
#30471=CARTESIAN_POINT('Ctrl Pts',(53.5286975798734,4.15516668331015,337.631306309879));
#30472=CARTESIAN_POINT('Ctrl Pts',(53.5209505014955,4.2285662621279,337.515399057528));
#30473=CARTESIAN_POINT('Ctrl Pts',(53.5132034231177,4.29713098390071,337.396388889458));
#30474=CARTESIAN_POINT('Ctrl Pts',(53.5054563447398,4.36059946924277,337.274720934827));
#30475=CARTESIAN_POINT('Ctrl Pts',(53.497709201434,4.42406848651186,337.153051960502));
#30476=CARTESIAN_POINT('Ctrl Pts',(53.4899620581282,4.48244100137742,337.028725501742));
#30477=CARTESIAN_POINT('Ctrl Pts',(53.4822149148224,4.53550186863297,336.902210782781));
#30478=CARTESIAN_POINT('Ctrl Pts',(53.4744660297943,4.58857466509797,336.775667620625));
#30479=CARTESIAN_POINT('Ctrl Pts',(53.4667171447662,4.63633328653853,336.646935579692));
#30480=CARTESIAN_POINT('Ctrl Pts',(53.4589682597381,4.67861110457458,336.516502949107));
#30481=CARTESIAN_POINT('Ctrl Pts',(53.4512111499634,4.72093379672353,336.385931875981));
#30482=CARTESIAN_POINT('Ctrl Pts',(53.4434540401886,4.75776394398962,336.253656979917));
#30483=CARTESIAN_POINT('Ctrl Pts',(53.4356969304139,4.78898495587991,336.120181304457));
#30484=CARTESIAN_POINT('Ctrl Pts',(53.4279356754877,4.82022265128067,335.986634303864));
#30485=CARTESIAN_POINT('Ctrl Pts',(53.4201744205615,4.84584516585099,335.851885629113));
#30486=CARTESIAN_POINT('Ctrl Pts',(53.4124131656354,4.86578743684675,335.716446565994));
#30487=CARTESIAN_POINT('Ctrl Pts',(53.4046394952307,4.88576160897694,335.580790844513));
#30488=CARTESIAN_POINT('Ctrl Pts',(53.396865824826,4.90003733921393,335.444442916706));
#30489=CARTESIAN_POINT('Ctrl Pts',(53.3890921544213,4.90860158300433,335.307918108963));
#30490=CARTESIAN_POINT('Ctrl Pts',(53.3816803502443,4.91676715918579,335.177748563867));
#30491=CARTESIAN_POINT('Ctrl Pts',(53.3742685460673,4.91974101528029,335.047418523487));
#30492=CARTESIAN_POINT('Ctrl Pts',(53.3668567418903,4.91755584867608,334.917371084651));
#30493=CARTESIAN_POINT('Ctrl Pts',(53.3590816631118,4.9152635805473,334.780949633446));
#30494=CARTESIAN_POINT('Ctrl Pts',(53.3513065843334,4.90728654049637,334.644408069534));
#30495=CARTESIAN_POINT('Ctrl Pts',(53.343531505555,4.89360540179282,334.508258976651));
#30496=CARTESIAN_POINT('Ctrl Pts',(53.335765994506,4.87994109860143,334.372277423895));
#30497=CARTESIAN_POINT('Ctrl Pts',(53.328000483457,4.86058670177242,334.236687766411));
#30498=CARTESIAN_POINT('Ctrl Pts',(53.320234972408,4.83557487546681,334.102002958661));
#30499=CARTESIAN_POINT('Ctrl Pts',(53.3124771608858,4.81058784845981,333.96745169129));
#30500=CARTESIAN_POINT('Ctrl Pts',(53.3047193493636,4.77995462582332,333.833803870079));
#30501=CARTESIAN_POINT('Ctrl Pts',(53.2969615378414,4.74375965743472,333.70156733906));
#30502=CARTESIAN_POINT('Ctrl Pts',(53.2892095643184,4.70759192690765,333.569430320225));
#30503=CARTESIAN_POINT('Ctrl Pts',(53.2814575907954,4.66587088421923,333.43870285313));
#30504=CARTESIAN_POINT('Ctrl Pts',(53.2737056172724,4.61873197221471,333.309882243351));
#30505=CARTESIAN_POINT('Ctrl Pts',(53.2659569267148,4.57161302356745,333.181116189176));
#30506=CARTESIAN_POINT('Ctrl Pts',(53.2582082361572,4.5190809031863,333.054255752452));
#30507=CARTESIAN_POINT('Ctrl Pts',(53.2504595455995,4.46132072818991,332.929782518013));
#30508=CARTESIAN_POINT('Ctrl Pts',(53.2427124672217,4.4035725706803,332.80533518127));
#30509=CARTESIAN_POINT('Ctrl Pts',(53.2349653888439,4.34059868657379,332.683274413223));
#30510=CARTESIAN_POINT('Ctrl Pts',(53.227218310466,4.27263194709239,332.564060898301));
#30511=CARTESIAN_POINT('Ctrl Pts',(53.2194711671602,4.20466463798429,332.444846384256));
#30512=CARTESIAN_POINT('Ctrl Pts',(53.2117240238545,4.13170458363291,332.328479510497));
#30513=CARTESIAN_POINT('Ctrl Pts',(53.2039768805487,4.05402993728916,332.215395121375));
#30514=CARTESIAN_POINT('Ctrl Pts',(53.1962279955206,3.97633782803589,332.102285308481));
#30515=CARTESIAN_POINT('Ctrl Pts',(53.1884791104925,3.89392923888849,331.992459770835));
#30516=CARTESIAN_POINT('Ctrl Pts',(53.1807302254644,3.80712461041235,331.886322871059));
#30517=CARTESIAN_POINT('Ctrl Pts',(53.1729731156896,3.72022784660662,331.780073316481));
#30518=CARTESIAN_POINT('Ctrl Pts',(53.1652160059149,3.62892597054433,331.677520523715));
#30519=CARTESIAN_POINT('Ctrl Pts',(53.1574588961402,3.53357890846681,331.579034761922));
#30520=CARTESIAN_POINT('Ctrl Pts',(53.149697641214,3.43818089596792,331.480496372486));
#30521=CARTESIAN_POINT('Ctrl Pts',(53.1419363862878,3.33873367348651,331.386029613567));
#30522=CARTESIAN_POINT('Ctrl Pts',(53.1341751313617,3.23563198296683,331.295965883891));
#30523=CARTESIAN_POINT('Ctrl Pts',(53.126401460957,3.13236536334307,331.205758081599));
#30524=CARTESIAN_POINT('Ctrl Pts',(53.1186277905524,3.02543289876756,331.119967628105));
#30525=CARTESIAN_POINT('Ctrl Pts',(53.1108541201477,2.91526087903867,331.038884365529));
#30526=CARTESIAN_POINT('Ctrl Pts',(53.1034423159706,2.81021739333343,330.961575548334));
#30527=CARTESIAN_POINT('Ctrl Pts',(53.0960305117935,2.70222940607966,330.888545706113));
#30528=CARTESIAN_POINT('Ctrl Pts',(53.0886187076163,2.59168722128641,330.820007128054));
#30529=CARTESIAN_POINT('Ctrl Pts',(53.0808436288379,2.47572703472884,330.748109270118));
#30530=CARTESIAN_POINT('Ctrl Pts',(53.0730685500595,2.35658948655505,330.680926858294));
#30531=CARTESIAN_POINT('Ctrl Pts',(53.0652934712811,2.23469516055991,330.618753533312));
#30532=CARTESIAN_POINT('Ctrl Pts',(53.057527960232,2.11295083329308,330.556656716564));
#30533=CARTESIAN_POINT('Ctrl Pts',(53.049762449183,1.98845682295723,330.499556897968));
#30534=CARTESIAN_POINT('Ctrl Pts',(53.041996938134,1.86166216035348,330.447704198626));
#30535=CARTESIAN_POINT('Ctrl Pts',(53.0342391266118,1.73499321502695,330.395902911386));
#30536=CARTESIAN_POINT('Ctrl Pts',(53.0264813150896,1.60602851641711,330.349338537065));
#30537=CARTESIAN_POINT('Ctrl Pts',(53.0187235035675,1.47524082207895,330.308214883504));
#30538=CARTESIAN_POINT('Ctrl Pts',(53.0109715300445,1.34455154962829,330.267122176797));
#30539=CARTESIAN_POINT('Ctrl Pts',(53.0032195565214,1.21204238344852,330.231462158087));
#30540=CARTESIAN_POINT('Ctrl Pts',(52.9954675829984,1.07820481430193,330.20139005118));
#30541=CARTESIAN_POINT('Ctrl Pts',(52.9877188924408,0.944423925445244,330.171330679827));
#30542=CARTESIAN_POINT('Ctrl Pts',(52.9799702018832,0.809316133124911,330.146854599018));
#30543=CARTESIAN_POINT('Ctrl Pts',(52.9722215113256,0.673386589796168,330.128066753004));
#30544=CARTESIAN_POINT('Ctrl Pts',(52.9644744329477,0.537485327744312,330.109282815959));
#30545=CARTESIAN_POINT('Ctrl Pts',(52.9567273545699,0.400763041709971,330.096184813157));
#30546=CARTESIAN_POINT('Ctrl Pts',(52.9489802761921,0.263733151039706,330.088826220999));
#30547=CARTESIAN_POINT('Ctrl Pts',(52.9412331328863,0.126702111927065,330.08146756717));
#30548=CARTESIAN_POINT('Ctrl Pts',(52.9334859895805,-0.0106361466516469,
330.079848440888));
#30549=CARTESIAN_POINT('Ctrl Pts',(52.9257388462747,-0.14776543012098,330.08397025638));
#30550=CARTESIAN_POINT('Ctrl Pts',(52.9179899612466,-0.284925543164574,
330.088092998543));
#30551=CARTESIAN_POINT('Ctrl Pts',(52.9102410762185,-0.421876196988287,
330.097959239058));
#30552=CARTESIAN_POINT('Ctrl Pts',(52.9024921911904,-0.558103945658428,
330.113518336437));
#30553=CARTESIAN_POINT('Ctrl Pts',(52.8947350814157,-0.694476287868504,
330.129093948402));
#30554=CARTESIAN_POINT('Ctrl Pts',(52.8869779716409,-0.83012380321036,330.150374443179));
#30555=CARTESIAN_POINT('Ctrl Pts',(52.8792208618662,-0.964540347707559,
330.177257525003));
#30556=CARTESIAN_POINT('Ctrl Pts',(52.87145960694,-1.09902872010824,330.204154972285));
#30557=CARTESIAN_POINT('Ctrl Pts',(52.8636983520138,-1.2322844314088,330.23666087953));
#30558=CARTESIAN_POINT('Ctrl Pts',(52.8559370970877,-1.36381518383249,330.274622638683));
#30559=CARTESIAN_POINT('Ctrl Pts',(52.848163426683,-1.49555634259439,330.312645124279));
#30560=CARTESIAN_POINT('Ctrl Pts',(52.8403897562784,-1.62556665756216,330.356140778003));
#30561=CARTESIAN_POINT('Ctrl Pts',(52.8326160858738,-1.7533717044416,330.404907973874));
#30562=CARTESIAN_POINT('Ctrl Pts',(52.8252042816966,-1.87522739564112,330.451405045045));
#30563=CARTESIAN_POINT('Ctrl Pts',(52.8177924775195,-1.99507824424029,330.502693809272));
#30564=CARTESIAN_POINT('Ctrl Pts',(52.8103806733424,-2.11253451583751,330.558560933448));
#30565=CARTESIAN_POINT('Ctrl Pts',(52.802605594564,-2.23574766918971,330.617166271799));
#30566=CARTESIAN_POINT('Ctrl Pts',(52.7948305157855,-2.35671495599475,330.680995319783));
#30567=CARTESIAN_POINT('Ctrl Pts',(52.7870554370071,-2.47496184547317,330.749853305361));
#30568=CARTESIAN_POINT('Ctrl Pts',(52.779289925958,-2.59306322462612,330.818626556804));
#30569=CARTESIAN_POINT('Ctrl Pts',(52.771524414909,-2.7084505327123,330.89241623783));
#30570=CARTESIAN_POINT('Ctrl Pts',(52.76375890386,-2.82067044122897,330.970980103738));
#30571=CARTESIAN_POINT('Ctrl Pts',(52.7560010923378,-2.93277908337955,331.049466073344));
#30572=CARTESIAN_POINT('Ctrl Pts',(52.7482432808156,-3.04172625756441,331.132716584938));
#30573=CARTESIAN_POINT('Ctrl Pts',(52.7404854692934,-3.14708474118129,331.220444378723));
#30574=CARTESIAN_POINT('Ctrl Pts',(52.7327334957704,-3.25236393919822,331.308106154562));
#30575=CARTESIAN_POINT('Ctrl Pts',(52.7249815222474,-3.35405952289839,331.400238257067));
#30576=CARTESIAN_POINT('Ctrl Pts',(52.7172295487243,-3.45177498742063,331.496511381677));
#30577=CARTESIAN_POINT('Ctrl Pts',(52.7094808581667,-3.54944906938555,331.592743734562));
#30578=CARTESIAN_POINT('Ctrl Pts',(52.701732167609,-3.64314610682035,331.693113347759));
#30579=CARTESIAN_POINT('Ctrl Pts',(52.6939834770514,-3.7325044828853,331.79725221915));
#30580=CARTESIAN_POINT('Ctrl Pts',(52.6862363986735,-3.82184426719377,331.901369423578));
#30581=CARTESIAN_POINT('Ctrl Pts',(52.6784893202957,-3.90684693127986,332.009254029867));
#30582=CARTESIAN_POINT('Ctrl Pts',(52.6707422419179,-3.98718966502875,332.120503231884));
#30583=CARTESIAN_POINT('Ctrl Pts',(52.6629950986121,-4.06753307212707,332.231753366277));
#30584=CARTESIAN_POINT('Ctrl Pts',(52.6552479553063,-4.14321624214478,332.346367835763));
#30585=CARTESIAN_POINT('Ctrl Pts',(52.6475008120004,-4.21395864332476,332.463913326629));
#30586=CARTESIAN_POINT('Ctrl Pts',(52.6397519269723,-4.28471694889842,332.581485244218));
#30587=CARTESIAN_POINT('Ctrl Pts',(52.6320030419442,-4.35053207377265,332.7019891596));
#30588=CARTESIAN_POINT('Ctrl Pts',(52.6242541569161,-4.41116874840035,332.824965900121));
#30589=CARTESIAN_POINT('Ctrl Pts',(52.6164970471414,-4.47186978342102,332.948073169425));
#30590=CARTESIAN_POINT('Ctrl Pts',(52.6087399373666,-4.52738121536722,333.073658155788));
#30591=CARTESIAN_POINT('Ctrl Pts',(52.6009828275918,-4.57751516338388,333.201239873832));
#30592=CARTESIAN_POINT('Ctrl Pts',(52.5932215726657,-4.62767590137936,333.328889767468));
#30593=CARTESIAN_POINT('Ctrl Pts',(52.5854603177395,-4.67245330208958,333.458538149585));
#30594=CARTESIAN_POINT('Ctrl Pts',(52.5776990628133,-4.71170928630875,333.589688451507));
#30595=CARTESIAN_POINT('Ctrl Pts',(52.5699253924086,-4.75102806730916,333.72104855117));
#30596=CARTESIAN_POINT('Ctrl Pts',(52.562151722004,-4.78480768557222,333.853914992686));
#30597=CARTESIAN_POINT('Ctrl Pts',(52.5543780515994,-4.81296095448017,333.987779711155));
#30598=CARTESIAN_POINT('Ctrl Pts',(52.5469662474224,-4.83980368194676,334.115412994772));
#30599=CARTESIAN_POINT('Ctrl Pts',(52.5395544432454,-4.86153203712724,334.243953423534));
#30600=CARTESIAN_POINT('Ctrl Pts',(52.5321426390684,-4.87811450873532,334.372957814684));
#30601=CARTESIAN_POINT('Ctrl Pts',(52.5202738422089,-4.90466863540197,334.579537329735));
#30602=CARTESIAN_POINT('Ctrl Pts',(52.5084050453495,-4.91810432005569,334.787838599102));
#30603=CARTESIAN_POINT('Ctrl Pts',(52.4965362484901,-4.91824882173174,334.996595586053));
#30604=CARTESIAN_POINT('',(55.9965362484619,-4.9182498257703,335.001309125831));
#30605=CARTESIAN_POINT('Ctrl Pts',(55.9965362484619,-4.9182498257703,335.001309125831));
#30606=CARTESIAN_POINT('Ctrl Pts',(55.9882359763961,-4.9182106052105,335.148656696918));
#30607=CARTESIAN_POINT('Ctrl Pts',(55.9799357043303,-4.91154550858833,335.295822679162));
#30608=CARTESIAN_POINT('Ctrl Pts',(55.9716354322645,-4.89832862073287,335.442221421699));
#30609=CARTESIAN_POINT('Ctrl Pts',(55.9632490671054,-4.8849746430628,335.59013865911));
#30610=CARTESIAN_POINT('Ctrl Pts',(55.9548627019463,-4.86493227844111,335.737272344221));
#30611=CARTESIAN_POINT('Ctrl Pts',(55.9464763367872,-4.83833005884191,335.883031881761));
#30612=CARTESIAN_POINT('Ctrl Pts',(55.9381312631354,-4.81185881919924,336.028073750694));
#30613=CARTESIAN_POINT('Ctrl Pts',(55.9297861894837,-4.77889233825748,336.17175470877));
#30614=CARTESIAN_POINT('Ctrl Pts',(55.9214411158319,-4.739606898083,336.313510378392));
#30615=CARTESIAN_POINT('Ctrl Pts',(55.9130341049192,-4.70002988078658,336.456318160706));
#30616=CARTESIAN_POINT('Ctrl Pts',(55.9046270940064,-4.6540398562618,336.597171677283));
#30617=CARTESIAN_POINT('Ctrl Pts',(55.8962200830937,-4.60186564622711,336.735515956877));
#30618=CARTESIAN_POINT('Ctrl Pts',(55.887813072181,-4.54969143619245,336.873860236471));
#30619=CARTESIAN_POINT('Ctrl Pts',(55.8794060612684,-4.49133322060517,337.009695028739));
#30620=CARTESIAN_POINT('Ctrl Pts',(55.8709990503557,-4.42706603779988,337.142491390755));
#30621=CARTESIAN_POINT('Ctrl Pts',(55.8632239715773,-4.36762964425063,337.265305811586));
#30622=CARTESIAN_POINT('Ctrl Pts',(55.8554488927988,-4.30298483270222,337.385839127243));
#30623=CARTESIAN_POINT('Ctrl Pts',(55.8476738140204,-4.23332957654058,337.503618133599));
#30624=CARTESIAN_POINT('Ctrl Pts',(55.8399083029714,-4.16376003560613,337.62125220539));
#30625=CARTESIAN_POINT('Ctrl Pts',(55.8321427919224,-4.08919251504711,337.736138378496));
#30626=CARTESIAN_POINT('Ctrl Pts',(55.8243772808734,-4.00987231659231,337.847824971294));
#30627=CARTESIAN_POINT('Ctrl Pts',(55.8166194693512,-3.93063076434522,337.959400826511));
#30628=CARTESIAN_POINT('Ctrl Pts',(55.8088616578289,-3.84664613680464,338.067783098033));
#30629=CARTESIAN_POINT('Ctrl Pts',(55.8011038463067,-3.75820857340413,338.172546513653));
#30630=CARTESIAN_POINT('Ctrl Pts',(55.7933518727837,-3.66983756207446,338.27723109148));
#30631=CARTESIAN_POINT('Ctrl Pts',(55.7855998992607,-3.57702053595824,338.37830193653));
#30632=CARTESIAN_POINT('Ctrl Pts',(55.7778479257377,-3.48008947077399,338.475364777676));
#30633=CARTESIAN_POINT('Ctrl Pts',(55.7700992351801,-3.38319945595352,338.57238651265));
#30634=CARTESIAN_POINT('Ctrl Pts',(55.7623505446224,-3.28219914300021,338.665403343712));
#30635=CARTESIAN_POINT('Ctrl Pts',(55.7546018540648,-3.17745896861545,338.75405614839));
#30636=CARTESIAN_POINT('Ctrl Pts',(55.7468547756869,-3.07274058629877,338.842690508112));
#30637=CARTESIAN_POINT('Ctrl Pts',(55.7391076973091,-2.9642841884288,338.926962395102));
#30638=CARTESIAN_POINT('Ctrl Pts',(55.7313606189313,-2.85249475275847,339.006551727856));
#30639=CARTESIAN_POINT('Ctrl Pts',(55.7236134756255,-2.740704380185,339.086141727645));
#30640=CARTESIAN_POINT('Ctrl Pts',(55.7158663323197,-2.62558123251232,339.161048868221));
#30641=CARTESIAN_POINT('Ctrl Pts',(55.7081191890139,-2.50756050875593,339.230995551573));
#30642=CARTESIAN_POINT('Ctrl Pts',(55.7003703039858,-2.38951325143526,339.300957960423));
#30643=CARTESIAN_POINT('Ctrl Pts',(55.6926214189576,-2.26856745793434,339.365957493646));
#30644=CARTESIAN_POINT('Ctrl Pts',(55.6848725339295,-2.14518387984355,339.4257619891));
#30645=CARTESIAN_POINT('Ctrl Pts',(55.6771154241548,-2.02166934114818,339.485629961663));
#30646=CARTESIAN_POINT('Ctrl Pts',(55.6693583143801,-1.89571220139915,339.540291710836));
#30647=CARTESIAN_POINT('Ctrl Pts',(55.6616012046053,-1.76779470426661,339.589562609451));
#30648=CARTESIAN_POINT('Ctrl Pts',(55.6538399496792,-1.63980885211362,339.638859836858));
#30649=CARTESIAN_POINT('Ctrl Pts',(55.646078694753,-1.5098609253601,339.682760348615));
#30650=CARTESIAN_POINT('Ctrl Pts',(55.6383174398268,-1.37844841417604,339.721129423343));
#30651=CARTESIAN_POINT('Ctrl Pts',(55.6305437694222,-1.24682568580134,339.759559876086));
#30652=CARTESIAN_POINT('Ctrl Pts',(55.6227700990175,-1.11373407093708,339.792441116084));
#30653=CARTESIAN_POINT('Ctrl Pts',(55.6149964286128,-0.979682211895785,
339.81968939105));
#30654=CARTESIAN_POINT('Ctrl Pts',(55.6075846244358,-0.851870499145784,
339.845669252259));
#30655=CARTESIAN_POINT('Ctrl Pts',(55.6001728202589,-0.723186213177062,
339.866528729482));
#30656=CARTESIAN_POINT('Ctrl Pts',(55.5927610160819,-0.594072739515768,
339.882239306165));
#30657=CARTESIAN_POINT('Ctrl Pts',(55.5849859373034,-0.458631029899123,
339.898719905011));
#30658=CARTESIAN_POINT('Ctrl Pts',(55.577210858525,-0.322288976450269,339.909586197146));
#30659=CARTESIAN_POINT('Ctrl Pts',(55.5694357797466,-0.185551641373691,
339.914748584707));
#30660=CARTESIAN_POINT('Ctrl Pts',(55.5616702686976,-0.0489825702929563,
339.919904619622));
#30661=CARTESIAN_POINT('Ctrl Pts',(55.5539047576486,0.0879804277186762,
339.919370701191));
#30662=CARTESIAN_POINT('Ctrl Pts',(55.5461392465996,0.224824777107929,339.913108678026));
#30663=CARTESIAN_POINT('Ctrl Pts',(55.5383814350773,0.361533444926443,339.906852863676));
#30664=CARTESIAN_POINT('Ctrl Pts',(55.5306236235551,0.498123310283324,339.894880264738));
#30665=CARTESIAN_POINT('Ctrl Pts',(55.5228658120329,0.634079741609925,339.877204726458));
#30666=CARTESIAN_POINT('Ctrl Pts',(55.5151138385099,0.769933861410248,339.85954248958));
#30667=CARTESIAN_POINT('Ctrl Pts',(55.5073618649869,0.905155109935398,339.836185905855));
#30668=CARTESIAN_POINT('Ctrl Pts',(55.4996098914638,1.03923228507392,339.807200778016));
#30669=CARTESIAN_POINT('Ctrl Pts',(55.4918612009062,1.17325267844926,339.778227925397));
#30670=CARTESIAN_POINT('Ctrl Pts',(55.4841125103486,1.30612958085206,339.743631352079));
#30671=CARTESIAN_POINT('Ctrl Pts',(55.476363819791,1.43736053397991,339.703528224414));
#30672=CARTESIAN_POINT('Ctrl Pts',(55.4686167414132,1.56856418341191,339.663433440539));
#30673=CARTESIAN_POINT('Ctrl Pts',(55.4608696630353,1.69812219115844,339.617834495325));
#30674=CARTESIAN_POINT('Ctrl Pts',(55.4531225846575,1.82554623715271,339.566898728735));
#30675=CARTESIAN_POINT('Ctrl Pts',(55.4453754413517,1.95297135108313,339.515962535254));
#30676=CARTESIAN_POINT('Ctrl Pts',(55.4376282980458,2.0782621046381,339.459689576268));
#30677=CARTESIAN_POINT('Ctrl Pts',(55.42988115474,2.20094954856742,339.398295595701));
#30678=CARTESIAN_POINT('Ctrl Pts',(55.4221322697119,2.32366457523886,339.336887812463));
#30679=CARTESIAN_POINT('Ctrl Pts',(55.4143833846839,2.44377477816129,339.270356891542));
#30680=CARTESIAN_POINT('Ctrl Pts',(55.4066344996558,2.56083558811472,339.198964652524));
#30681=CARTESIAN_POINT('Ctrl Pts',(55.398877389881,2.67802064762139,339.127496637045));
#30682=CARTESIAN_POINT('Ctrl Pts',(55.3911202801063,2.79214951439594,339.051157200021));
#30683=CARTESIAN_POINT('Ctrl Pts',(55.3833631703315,2.90280596179214,338.970251958086));
#30684=CARTESIAN_POINT('Ctrl Pts',(55.3756019154054,3.01352154045571,338.889303482976));
#30685=CARTESIAN_POINT('Ctrl Pts',(55.3678406604792,3.12076069694579,338.803784584974));
#30686=CARTESIAN_POINT('Ctrl Pts',(55.360079405553,3.22414092070293,338.714040708709));
#30687=CARTESIAN_POINT('Ctrl Pts',(55.3523057351483,3.32768651912647,338.624153271489));
#30688=CARTESIAN_POINT('Ctrl Pts',(55.3445320647436,3.42736056492973,338.530027618853));
#30689=CARTESIAN_POINT('Ctrl Pts',(55.336758394339,3.52281737348578,338.432046155804));
#30690=CARTESIAN_POINT('Ctrl Pts',(55.3293465901619,3.61383064463764,338.338625753433));
#30691=CARTESIAN_POINT('Ctrl Pts',(55.3219347859849,3.70101027509299,338.241700652043));
#30692=CARTESIAN_POINT('Ctrl Pts',(55.3145229818078,3.78409234332512,338.141628272041));
#30693=CARTESIAN_POINT('Ctrl Pts',(55.3067479030294,3.87124651121026,338.036651046595));
#30694=CARTESIAN_POINT('Ctrl Pts',(55.2989728242509,3.95416671651489,337.927878479301));
#30695=CARTESIAN_POINT('Ctrl Pts',(55.2911977454725,4.03250429634635,337.815686801199));
#30696=CARTESIAN_POINT('Ctrl Pts',(55.2834322344235,4.11074547679861,337.7036331821));
#30697=CARTESIAN_POINT('Ctrl Pts',(55.2756667233745,4.18441503055797,337.588169141195));
#30698=CARTESIAN_POINT('Ctrl Pts',(55.2679012123255,4.25320349126631,337.469705068299));
#30699=CARTESIAN_POINT('Ctrl Pts',(55.2601434008033,4.32192374801559,337.351358452875));
#30700=CARTESIAN_POINT('Ctrl Pts',(55.2523855892811,4.38577234781364,337.230018060807));
#30701=CARTESIAN_POINT('Ctrl Pts',(55.2446277777589,4.44448243675132,337.106124149216));
#30702=CARTESIAN_POINT('Ctrl Pts',(55.2368758042359,4.50314834448523,336.982323471722));
#30703=CARTESIAN_POINT('Ctrl Pts',(55.2291238307129,4.5566832715103,336.855973451364));
#30704=CARTESIAN_POINT('Ctrl Pts',(55.2213718571899,4.60486591195454,336.727539578539));
#30705=CARTESIAN_POINT('Ctrl Pts',(55.2136231666322,4.65302814702194,336.599160097536));
#30706=CARTESIAN_POINT('Ctrl Pts',(55.2058744760746,4.69584246679902,336.468698884528));
#30707=CARTESIAN_POINT('Ctrl Pts',(55.198125785517,4.73313548995022,336.336641872857));
#30708=CARTESIAN_POINT('Ctrl Pts',(55.1903787071392,4.77042075397648,336.204612336749));
#30709=CARTESIAN_POINT('Ctrl Pts',(55.1826316287614,4.80218690016365,336.070988038314));
#30710=CARTESIAN_POINT('Ctrl Pts',(55.1748845503835,4.82831039024877,335.936270173569));
#30711=CARTESIAN_POINT('Ctrl Pts',(55.1671374070777,4.85443409927388,335.801551179759));
#30712=CARTESIAN_POINT('Ctrl Pts',(55.1593902637719,4.87491498346233,335.665738985085));
#30713=CARTESIAN_POINT('Ctrl Pts',(55.1516431204661,4.88968069113446,335.529344690393));
#30714=CARTESIAN_POINT('Ctrl Pts',(55.143894235438,4.90444971845117,335.392919731367));
#30715=CARTESIAN_POINT('Ctrl Pts',(55.1361453504099,4.91350097039693,335.255912800437));
#30716=CARTESIAN_POINT('Ctrl Pts',(55.1283964653818,4.91681403473352,335.118839430946));
#30717=CARTESIAN_POINT('Ctrl Pts',(55.1206393556071,4.92013061559083,334.981620570364));
#30718=CARTESIAN_POINT('Ctrl Pts',(55.1128822458324,4.91769683289119,334.844335521731));
#30719=CARTESIAN_POINT('Ctrl Pts',(55.1051251360576,4.90954444206203,334.707499685611));
#30720=CARTESIAN_POINT('Ctrl Pts',(55.0973638811315,4.90138769485587,334.570590728795));
#30721=CARTESIAN_POINT('Ctrl Pts',(55.0896026262053,4.88750629001892,334.434131851474));
#30722=CARTESIAN_POINT('Ctrl Pts',(55.0818413712792,4.86798372089684,334.298631654846));
#30723=CARTESIAN_POINT('Ctrl Pts',(55.0740677008745,4.84842992202655,334.162914702064));
#30724=CARTESIAN_POINT('Ctrl Pts',(55.0662940304698,4.82321699812177,334.028159878925));
#30725=CARTESIAN_POINT('Ctrl Pts',(55.0585203600652,4.79247945192098,333.894864820298));
#30726=CARTESIAN_POINT('Ctrl Pts',(55.0511085558881,4.76317274589082,333.767774678718));
#30727=CARTESIAN_POINT('Ctrl Pts',(55.043696751711,4.72884426073161,333.642011733649));
#30728=CARTESIAN_POINT('Ctrl Pts',(55.0362849475339,4.68965173580566,333.517991343023));
#30729=CARTESIAN_POINT('Ctrl Pts',(55.0285098687555,4.64853826848464,333.387892343615));
#30730=CARTESIAN_POINT('Ctrl Pts',(55.020734789977,4.60194197713734,333.259299896418));
#30731=CARTESIAN_POINT('Ctrl Pts',(55.0129597111986,4.54999056097327,333.132710799701));
#30732=CARTESIAN_POINT('Ctrl Pts',(55.0051942001496,4.49810307433418,333.006277478926));
#30733=CARTESIAN_POINT('Ctrl Pts',(54.9974286891007,4.44087372171737,332.88184296164));
#30734=CARTESIAN_POINT('Ctrl Pts',(54.9896631780516,4.37848013866901,332.759889570182));
#30735=CARTESIAN_POINT('Ctrl Pts',(54.9819053665294,4.31614841903985,332.638057095866));
#30736=CARTESIAN_POINT('Ctrl Pts',(54.9741475550072,4.24866283564847,332.518701197487));
#30737=CARTESIAN_POINT('Ctrl Pts',(54.966389743485,4.17624920013888,332.402284526581));
#30738=CARTESIAN_POINT('Ctrl Pts',(54.958637769962,4.10389005818644,332.285955462912));
#30739=CARTESIAN_POINT('Ctrl Pts',(54.950885796439,4.02661045135484,332.172561554681));
#30740=CARTESIAN_POINT('Ctrl Pts',(54.943133822916,3.9446820591438,332.06254080628));
#30741=CARTESIAN_POINT('Ctrl Pts',(54.9353851323583,3.86278836365551,331.952566651732));
#30742=CARTESIAN_POINT('Ctrl Pts',(54.9276364418008,3.77625003148594,331.845963128607));
#30743=CARTESIAN_POINT('Ctrl Pts',(54.9198877512432,3.6853818677589,331.743139003382));
#30744=CARTESIAN_POINT('Ctrl Pts',(54.9121406728653,3.59453260991228,331.640336271575));
#30745=CARTESIAN_POINT('Ctrl Pts',(54.9043935944875,3.49935557105182,331.541311666301));
#30746=CARTESIAN_POINT('Ctrl Pts',(54.8966465161097,3.4002053639589,331.446440299445));
#30747=CARTESIAN_POINT('Ctrl Pts',(54.8888993728038,3.30105432589182,331.351568137476));
#30748=CARTESIAN_POINT('Ctrl Pts',(54.881152229498,3.19793033559151,331.260849553582));
#30749=CARTESIAN_POINT('Ctrl Pts',(54.8734050861922,3.09122403501736,331.174621975826));
#30750=CARTESIAN_POINT('Ctrl Pts',(54.8656562011641,2.98449374460147,331.088375012281));
#30751=CARTESIAN_POINT('Ctrl Pts',(54.8579073161361,2.8741798452564,331.006621309638));
#30752=CARTESIAN_POINT('Ctrl Pts',(54.850158431108,2.7607048137354,330.929657017656));
#30753=CARTESIAN_POINT('Ctrl Pts',(54.8424013213333,2.64710933864345,330.852611034979));
#30754=CARTESIAN_POINT('Ctrl Pts',(54.8346442115585,2.53034635293069,330.780364837544));
#30755=CARTESIAN_POINT('Ctrl Pts',(54.8268871017838,2.41086645261118,330.713170634353));
#30756=CARTESIAN_POINT('Ctrl Pts',(54.8191258468576,2.29132270605309,330.645940524728));
#30757=CARTESIAN_POINT('Ctrl Pts',(54.8113645919315,2.16905950021886,330.583767965675));
#30758=CARTESIAN_POINT('Ctrl Pts',(54.8036033370053,2.0445497117483,330.52685797915));
#30759=CARTESIAN_POINT('Ctrl Pts',(54.7958296666006,1.91984074819393,330.469856955195));
#30760=CARTESIAN_POINT('Ctrl Pts',(54.788055996196,1.79287838270644,330.41813547377));
#30761=CARTESIAN_POINT('Ctrl Pts',(54.7802823257913,1.6641538742119,330.371849727435));
#30762=CARTESIAN_POINT('Ctrl Pts',(54.7728705216142,1.54142152255667,330.327718593727));
#30763=CARTESIAN_POINT('Ctrl Pts',(54.7654587174371,1.41708766592525,330.28852860341));
#30764=CARTESIAN_POINT('Ctrl Pts',(54.75804691326,1.29158694948444,330.2543718841));
#30765=CARTESIAN_POINT('Ctrl Pts',(54.7502718344816,1.1599350690839,330.218541042229));
#30766=CARTESIAN_POINT('Ctrl Pts',(54.7424967557031,1.02658300989388,330.1881361059));
#30767=CARTESIAN_POINT('Ctrl Pts',(54.7347216769247,0.892017645546317,330.163318536172));
#30768=CARTESIAN_POINT('Ctrl Pts',(54.7269561658757,0.757617872446341,330.138531506045));
#30769=CARTESIAN_POINT('Ctrl Pts',(54.7191906548266,0.622008145645764,330.11931823224));
#30770=CARTESIAN_POINT('Ctrl Pts',(54.7114251437776,0.485690189076216,330.105790349532));
#30771=CARTESIAN_POINT('Ctrl Pts',(54.7036673322554,0.349507392157486,330.092275879759));
#30772=CARTESIAN_POINT('Ctrl Pts',(54.6959095207333,0.212618149369224,330.084435621322));
#30773=CARTESIAN_POINT('Ctrl Pts',(54.6881517092111,0.0755337138958797,
330.082330051685));
#30774=CARTESIAN_POINT('Ctrl Pts',(54.6803997356881,-0.0614475611925734,
330.080226066555));
#30775=CARTESIAN_POINT('Ctrl Pts',(54.6726477621651,-0.198623347336834,
330.083848186343));
#30776=CARTESIAN_POINT('Ctrl Pts',(54.664895788642,-0.335478295932384,330.09320497927));
#30777=CARTESIAN_POINT('Ctrl Pts',(54.6571470980844,-0.472275286375859,
330.10255780959));
#30778=CARTESIAN_POINT('Ctrl Pts',(54.6493984075268,-0.608751320363877,
330.117640456054));
#30779=CARTESIAN_POINT('Ctrl Pts',(54.6416497169692,-0.744392298328861,
330.138409399313));
#30780=CARTESIAN_POINT('Ctrl Pts',(54.6339026385913,-0.880005055055391,
330.15917402142));
#30781=CARTESIAN_POINT('Ctrl Pts',(54.6261555602135,-1.01478271521205,330.185622527967));
#30782=CARTESIAN_POINT('Ctrl Pts',(54.6184084818356,-1.14821793788851,330.217659712065));
#30783=CARTESIAN_POINT('Ctrl Pts',(54.6106613385298,-1.28165427888065,330.249697164665));
#30784=CARTESIAN_POINT('Ctrl Pts',(54.6029141952241,-1.41374777987883,330.287323296986));
#30785=CARTESIAN_POINT('Ctrl Pts',(54.5951670519183,-1.54400329164488,330.330392211557));
#30786=CARTESIAN_POINT('Ctrl Pts',(54.5874181668902,-1.67428808761519,330.373470808934));
#30787=CARTESIAN_POINT('Ctrl Pts',(54.5796692818621,-1.80273370105262,330.421994500811));
#30788=CARTESIAN_POINT('Ctrl Pts',(54.571920396834,-1.92886246689311,330.475768281099));
#30789=CARTESIAN_POINT('Ctrl Pts',(54.5641632870593,-2.05512510710899,330.529599137433));
#30790=CARTESIAN_POINT('Ctrl Pts',(54.5564061772845,-2.1790656272652,330.58869106023));
#30791=CARTESIAN_POINT('Ctrl Pts',(54.5486490675098,-2.30022809607237,330.652801618451));
#30792=CARTESIAN_POINT('Ctrl Pts',(54.5408878125836,-2.42145531022877,330.716946435305));
#30793=CARTESIAN_POINT('Ctrl Pts',(54.5331265576575,-2.53990117766808,330.786115034298));
#30794=CARTESIAN_POINT('Ctrl Pts',(54.5253653027313,-2.65513739036905,330.86002071252));
#30795=CARTESIAN_POINT('Ctrl Pts',(54.5175916323266,-2.77055794345502,330.934044615741));
#30796=CARTESIAN_POINT('Ctrl Pts',(54.509817961922,-2.88275826167886,331.012820516126));
#30797=CARTESIAN_POINT('Ctrl Pts',(54.5020442915173,-2.99134115099241,331.096019828319));
#30798=CARTESIAN_POINT('Ctrl Pts',(54.4946324873402,-3.09486948068459,331.175346192512));
#30799=CARTESIAN_POINT('Ctrl Pts',(54.4872206831632,-3.19510936372162,331.258693232618));
#30800=CARTESIAN_POINT('Ctrl Pts',(54.4798088789861,-3.29174811658647,331.345745301782));
#30801=CARTESIAN_POINT('Ctrl Pts',(54.4721496015553,-3.39161354760378,331.435703958638));
#30802=CARTESIAN_POINT('Ctrl Pts',(54.4644903241245,-3.4879690371342,331.529922246825));
#30803=CARTESIAN_POINT('Ctrl Pts',(54.4568310466937,-3.58042108453715,331.628091353565));
#30804=CARTESIAN_POINT('Ctrl Pts',(54.449181280803,-3.672758321977,331.726138550712));
#30805=CARTESIAN_POINT('Ctrl Pts',(54.4415315149124,-3.7612014832035,331.828126518954));
#30806=CARTESIAN_POINT('Ctrl Pts',(54.4338817490217,-3.84539041192421,331.933706530291));
#30807=CARTESIAN_POINT('Ctrl Pts',(54.4260756865019,-3.93129945155538,332.041443705665));
#30808=CARTESIAN_POINT('Ctrl Pts',(54.418269623982,-4.01277819006488,332.152921045607));
#30809=CARTESIAN_POINT('Ctrl Pts',(54.4104635614622,-4.08948322967486,332.267728055865));
#30810=CARTESIAN_POINT('Ctrl Pts',(54.4028272154001,-4.16452057733722,332.380038975546));
#30811=CARTESIAN_POINT('Ctrl Pts',(54.3951908693379,-4.23498942841753,332.495535914817));
#30812=CARTESIAN_POINT('Ctrl Pts',(54.3875545232757,-4.30060931046474,332.613801638328));
#30813=CARTESIAN_POINT('Ctrl Pts',(54.3799211644284,-4.36620352307743,332.732021098205));
#30814=CARTESIAN_POINT('Ctrl Pts',(54.372287805581,-4.42695234296321,332.853006836397));
#30815=CARTESIAN_POINT('Ctrl Pts',(54.3646544467337,-4.48261975490676,332.976314452436));
#30816=CARTESIAN_POINT('Ctrl Pts',(54.3570223074505,-4.5382782729964,333.099602367902));
#30817=CARTESIAN_POINT('Ctrl Pts',(54.3493901681673,-4.58885683266491,333.225211055429));
#30818=CARTESIAN_POINT('Ctrl Pts',(54.3417580288841,-4.63416658944166,333.352673959472));
#30819=CARTESIAN_POINT('Ctrl Pts',(54.3338228805226,-4.68127522162277,333.4851973604));
#30820=CARTESIAN_POINT('Ctrl Pts',(54.325887732161,-4.72268787865864,333.61972481477));
#30821=CARTESIAN_POINT('Ctrl Pts',(54.3179525837995,-4.75824888827521,333.755712822646));
#30822=CARTESIAN_POINT('Ctrl Pts',(54.3103144412865,-4.79247887957251,333.886610915144));
#30823=CARTESIAN_POINT('Ctrl Pts',(54.3026762987735,-4.82128732478986,334.018861780984));
#30824=CARTESIAN_POINT('Ctrl Pts',(54.2950381562605,-4.84458745902484,334.151969685472));
#30825=CARTESIAN_POINT('Ctrl Pts',(54.2873966328377,-4.86789790671672,334.285136508187));
#30826=CARTESIAN_POINT('Ctrl Pts',(54.2797551094148,-4.88569513531771,334.419160725621));
#30827=CARTESIAN_POINT('Ctrl Pts',(54.2721135859919,-4.89794422320548,334.553541212576));
#30828=CARTESIAN_POINT('Ctrl Pts',(54.2644640690337,-4.91020612444362,334.688062270346));
#30829=CARTESIAN_POINT('Ctrl Pts',(54.2568145520755,-4.91690828641832,334.822939939611));
#30830=CARTESIAN_POINT('Ctrl Pts',(54.2491650351173,-4.91806785985879,334.957672841768));
#30831=CARTESIAN_POINT('Ctrl Pts',(54.2482887729268,-4.91820069051574,334.973106672246));
#30832=CARTESIAN_POINT('Ctrl Pts',(54.2474125107363,-4.91826084731576,334.988538608389));
#30833=CARTESIAN_POINT('Ctrl Pts',(54.2465362485458,-4.9182483994059,335.00396790137));
#30834=CARTESIAN_POINT('',(57.746536723243,-4.91737005110712,334.995488220275));
#30835=CARTESIAN_POINT('Ctrl Pts',(57.7465362484901,-4.91824793749837,334.995495802735));
#30836=CARTESIAN_POINT('Ctrl Pts',(57.7388648584507,-4.91837207600807,335.131045809413));
#30837=CARTESIAN_POINT('Ctrl Pts',(57.7311934684114,-4.91288823446128,335.266732526264));
#30838=CARTESIAN_POINT('Ctrl Pts',(57.7235220783721,-4.90178935935022,335.402049921106));
#30839=CARTESIAN_POINT('Ctrl Pts',(57.7158548430756,-4.89069649527138,335.537294029491));
#30840=CARTESIAN_POINT('Ctrl Pts',(57.7081876077791,-4.87399467829062,335.672168816094));
#30841=CARTESIAN_POINT('Ctrl Pts',(57.7005203724827,-4.85172892970453,335.806169619353));
#30842=CARTESIAN_POINT('Ctrl Pts',(57.6928552568424,-4.82946933662675,335.940133377235));
#30843=CARTESIAN_POINT('Ctrl Pts',(57.6851901412021,-4.80164893564545,336.073223237912));
#30844=CARTESIAN_POINT('Ctrl Pts',(57.6775250255618,-4.76836440272733,336.204941486257));
#30845=CARTESIAN_POINT('Ctrl Pts',(57.6698602841005,-4.73508149462132,336.336653304666));
#30846=CARTESIAN_POINT('Ctrl Pts',(57.6621955426392,-4.6963350830001,336.466993256056));
#30847=CARTESIAN_POINT('Ctrl Pts',(57.6545308011779,-4.65227245534205,336.595476124474));
#30848=CARTESIAN_POINT('Ctrl Pts',(57.6468646889625,-4.60820194757135,336.723981970628));
#30849=CARTESIAN_POINT('Ctrl Pts',(57.6391985767472,-4.55881346291096,336.850629695007));
#30850=CARTESIAN_POINT('Ctrl Pts',(57.6315324645318,-4.50430324539716,336.974951983215));
#30851=CARTESIAN_POINT('Ctrl Pts',(57.6238584954147,-4.44973716104893,337.099401687768));
#30852=CARTESIAN_POINT('Ctrl Pts',(57.6161845262976,-4.39003902030269,337.221520828921));
#30853=CARTESIAN_POINT('Ctrl Pts',(57.6085105571805,-4.32545224267202,337.340864361484));
#30854=CARTESIAN_POINT('Ctrl Pts',(57.600832649253,-4.26083231465094,337.460269149381));
#30855=CARTESIAN_POINT('Ctrl Pts',(57.5931547413254,-4.19131895732629,337.576895148148));
#30856=CARTESIAN_POINT('Ctrl Pts',(57.5854768333979,-4.11719949279303,337.69032551916));
#30857=CARTESIAN_POINT('Ctrl Pts',(57.5777866395038,-4.04296142443203,337.803937398178));
#30858=CARTESIAN_POINT('Ctrl Pts',(57.5700964456096,-3.9641027559769,337.914343107769));
#30859=CARTESIAN_POINT('Ctrl Pts',(57.5624062517154,-3.88095219500436,338.021157579901));
#30860=CARTESIAN_POINT('Ctrl Pts',(57.5550799198101,-3.801735907849,338.122918118828));
#30861=CARTESIAN_POINT('Ctrl Pts',(57.5477535879048,-3.71862476919697,338.221419264264));
#30862=CARTESIAN_POINT('Ctrl Pts',(57.5404272559994,-3.63193320562401,338.316360090881));
#30863=CARTESIAN_POINT('Ctrl Pts',(57.532652177221,-3.5399316767669,338.417116160326));
#30864=CARTESIAN_POINT('Ctrl Pts',(57.5248770984425,-3.44358887110002,338.514200122131));
#30865=CARTESIAN_POINT('Ctrl Pts',(57.5171020196641,-3.34322952508125,338.60721490975));
#30866=CARTESIAN_POINT('Ctrl Pts',(57.5093365086151,-3.24299367762721,338.700115236752));
#30867=CARTESIAN_POINT('Ctrl Pts',(57.5015709975661,-3.13875140813542,338.788956089653));
#30868=CARTESIAN_POINT('Ctrl Pts',(57.4938054865171,-3.03086667518702,338.873374531302));
#30869=CARTESIAN_POINT('Ctrl Pts',(57.4860476749949,-2.92308891026529,338.95770927182));
#30870=CARTESIAN_POINT('Ctrl Pts',(57.4782898634727,-2.81167617485285,339.037630087828));
#30871=CARTESIAN_POINT('Ctrl Pts',(57.4705320519505,-2.69702786843564,339.112812144918));
#30872=CARTESIAN_POINT('Ctrl Pts',(57.4627800784275,-2.58246583850456,339.187937625125));
#30873=CARTESIAN_POINT('Ctrl Pts',(57.4550281049045,-2.46467340960457,339.258331231013));
#30874=CARTESIAN_POINT('Ctrl Pts',(57.4472761313815,-2.3440812355723,339.323709775591));
#30875=CARTESIAN_POINT('Ctrl Pts',(57.4395274408238,-2.22354013239741,339.389060632316));
#30876=CARTESIAN_POINT('Ctrl Pts',(57.4317787502662,-2.10020198526002,339.449400466076));
#30877=CARTESIAN_POINT('Ctrl Pts',(57.4240300597086,-1.97452428413207,339.504490749671));
#30878=CARTESIAN_POINT('Ctrl Pts',(57.4162829813308,-1.8488727312996,339.559569571273));
#30879=CARTESIAN_POINT('Ctrl Pts',(57.408535902953,-1.72088295045042,339.609400858372));
#30880=CARTESIAN_POINT('Ctrl Pts',(57.4007888245751,-1.59103440029527,339.653793355917));
#30881=CARTESIAN_POINT('Ctrl Pts',(57.3930416812693,-1.46118476188429,339.698186225513));
#30882=CARTESIAN_POINT('Ctrl Pts',(57.3852945379635,-1.3294766929521,339.737140088191));
#30883=CARTESIAN_POINT('Ctrl Pts',(57.3775473946577,-1.19640649861654,339.770513028236));
#30884=CARTESIAN_POINT('Ctrl Pts',(57.3697985096296,-1.06330638727604,339.803893471226));
#30885=CARTESIAN_POINT('Ctrl Pts',(57.3620496246015,-0.928843920218223,
339.831690399787));
#30886=CARTESIAN_POINT('Ctrl Pts',(57.3543007395734,-0.793526932057894,
339.853812735428));
#30887=CARTESIAN_POINT('Ctrl Pts',(57.3465436297987,-0.658066317048245,
339.875958551944));
#30888=CARTESIAN_POINT('Ctrl Pts',(57.3387865200239,-0.521749755485907,
339.892417680725));
#30889=CARTESIAN_POINT('Ctrl Pts',(57.3310294102492,-0.385092120905921,
339.90315073406));
#30890=CARTESIAN_POINT('Ctrl Pts',(57.3232681553231,-0.248361460855573,
339.913889522796));
#30891=CARTESIAN_POINT('Ctrl Pts',(57.3155069003969,-0.11128975503674,339.918896124835));
#30892=CARTESIAN_POINT('Ctrl Pts',(57.3077456454707,0.0256077464752018,
339.918183333897));
#30893=CARTESIAN_POINT('Ctrl Pts',(57.2999719750661,0.162724239374864,339.917469402726));
#30894=CARTESIAN_POINT('Ctrl Pts',(57.2921983046614,0.299665580455625,339.911017814241));
#30895=CARTESIAN_POINT('Ctrl Pts',(57.2844246342567,0.43592037065603,339.898893394732));
#30896=CARTESIAN_POINT('Ctrl Pts',(57.2770128300797,0.565832467591508,339.887333369868));
#30897=CARTESIAN_POINT('Ctrl Pts',(57.2696010259026,0.695120207681032,339.870616805978));
#30898=CARTESIAN_POINT('Ctrl Pts',(57.2621892217255,0.823350494014021,339.848842854384));
#30899=CARTESIAN_POINT('Ctrl Pts',(57.2544141429471,0.957865728658688,339.82600169656));
#30900=CARTESIAN_POINT('Ctrl Pts',(57.2466390641686,1.0916423236309,339.7975226783));
#30901=CARTESIAN_POINT('Ctrl Pts',(57.2388639853902,1.22417064367228,339.763464001929));
#30902=CARTESIAN_POINT('Ctrl Pts',(57.2310984743412,1.3565358791786,339.729447236927));
#30903=CARTESIAN_POINT('Ctrl Pts',(57.2233329632922,1.48765552116257,339.689864571792));
#30904=CARTESIAN_POINT('Ctrl Pts',(57.2155674522432,1.61702740915682,339.644825660941));
#30905=CARTESIAN_POINT('Ctrl Pts',(57.2078096407209,1.74627102454782,339.599831406301));
#30906=CARTESIAN_POINT('Ctrl Pts',(57.2000518291988,1.87376996775819,339.549391799604));
#30907=CARTESIAN_POINT('Ctrl Pts',(57.1922940176765,1.99903494062448,339.493666917859));
#30908=CARTESIAN_POINT('Ctrl Pts',(57.1845420441536,2.12420564762537,339.437983970856));
#30909=CARTESIAN_POINT('Ctrl Pts',(57.1767900706306,2.24714537480343,339.377023823733));
#30910=CARTESIAN_POINT('Ctrl Pts',(57.1690380971076,2.36738293267486,339.31099537376));
#30911=CARTESIAN_POINT('Ctrl Pts',(57.16128940655,2.48756956986963,339.244994886874));
#30912=CARTESIAN_POINT('Ctrl Pts',(57.1535407159924,2.60505597192953,339.173930553989));
#30913=CARTESIAN_POINT('Ctrl Pts',(57.1457920254348,2.71939398216957,339.098058007427));
#30914=CARTESIAN_POINT('Ctrl Pts',(57.138044947057,2.8337082034316,339.022201246783));
#30915=CARTESIAN_POINT('Ctrl Pts',(57.1302978686791,2.94487501032733,338.941538478293));
#30916=CARTESIAN_POINT('Ctrl Pts',(57.1225507903013,3.05247410978212,338.856369389933));
#30917=CARTESIAN_POINT('Ctrl Pts',(57.1148036469955,3.16007411102093,338.771199587773));
#30918=CARTESIAN_POINT('Ctrl Pts',(57.1070565036897,3.26410603869727,338.681523633007));
#30919=CARTESIAN_POINT('Ctrl Pts',(57.0993093603839,3.3641819736827,338.587682080459));
#30920=CARTESIAN_POINT('Ctrl Pts',(57.0915604753558,3.46428040786298,338.493819430338));
#30921=CARTESIAN_POINT('Ctrl Pts',(57.0838115903277,3.56042079449067,338.39578958619));
#30922=CARTESIAN_POINT('Ctrl Pts',(57.0760627052996,3.65225172527092,338.293970309179));
#30923=CARTESIAN_POINT('Ctrl Pts',(57.0683055955249,3.74418012634996,338.192042960136));
#30924=CARTESIAN_POINT('Ctrl Pts',(57.0605484857502,3.83178967218643,338.08631843434));
#30925=CARTESIAN_POINT('Ctrl Pts',(57.0527913759754,3.9147686132002,337.977208384981));
#30926=CARTESIAN_POINT('Ctrl Pts',(57.0450301210493,3.99779189550695,337.8680400307));
#30927=CARTESIAN_POINT('Ctrl Pts',(57.0372688661231,4.07617941916421,337.755482868623));
#30928=CARTESIAN_POINT('Ctrl Pts',(57.0295076111969,4.14966311130294,337.639977106945));
#30929=CARTESIAN_POINT('Ctrl Pts',(57.0217339407923,4.22326435340077,337.524286573691));
#30930=CARTESIAN_POINT('Ctrl Pts',(57.0139602703876,4.29194589235666,337.40563835374));
#30931=CARTESIAN_POINT('Ctrl Pts',(57.006186599983,4.35548549460405,337.284497574696));
#30932=CARTESIAN_POINT('Ctrl Pts',(56.9987747958058,4.41606731308076,337.168995928061));
#30933=CARTESIAN_POINT('Ctrl Pts',(56.9913629916286,4.47197501256549,337.051228817268));
#30934=CARTESIAN_POINT('Ctrl Pts',(56.9839511874514,4.52305759793053,336.931614099219));
#30935=CARTESIAN_POINT('Ctrl Pts',(56.976176108673,4.57664389297102,336.806136707526));
#30936=CARTESIAN_POINT('Ctrl Pts',(56.9684010298945,4.62508947058191,336.678229483909));
#30937=CARTESIAN_POINT('Ctrl Pts',(56.9606259511161,4.66816748145873,336.548352488147));
#30938=CARTESIAN_POINT('Ctrl Pts',(56.9528604400671,4.7111924821006,336.418635314297));
#30939=CARTESIAN_POINT('Ctrl Pts',(56.945094929018,4.74886293645054,336.28695355868));
#30940=CARTESIAN_POINT('Ctrl Pts',(56.937329417969,4.78099930740395,336.153788839044));
#30941=CARTESIAN_POINT('Ctrl Pts',(56.9295716064468,4.81310381505205,336.020756152615));
#30942=CARTESIAN_POINT('Ctrl Pts',(56.9218137949246,4.83968506775702,335.886243805791));
#30943=CARTESIAN_POINT('Ctrl Pts',(56.9140559834024,4.86061289038045,335.750749886692));
#30944=CARTESIAN_POINT('Ctrl Pts',(56.9063040098794,4.88152496415359,335.615357931064));
#30945=CARTESIAN_POINT('Ctrl Pts',(56.8985520363564,4.89679201656638,335.478986258175));
#30946=CARTESIAN_POINT('Ctrl Pts',(56.8908000628334,4.90633472612238,335.342144147613));
#30947=CARTESIAN_POINT('Ctrl Pts',(56.8830513722758,4.91587339433525,335.205359989765));
#30948=CARTESIAN_POINT('Ctrl Pts',(56.8753026817182,4.91969251424371,335.068106179615));
#30949=CARTESIAN_POINT('Ctrl Pts',(56.8675539911605,4.91776452922478,334.930897919));
#30950=CARTESIAN_POINT('Ctrl Pts',(56.8598069127827,4.91583694533923,334.793718205708));
#30951=CARTESIAN_POINT('Ctrl Pts',(56.8520598344048,4.90816464041253,334.656584413691));
#30952=CARTESIAN_POINT('Ctrl Pts',(56.844312756027,4.89477218375724,334.52001215472));
#30953=CARTESIAN_POINT('Ctrl Pts',(56.8365656127212,4.88137961486029,334.383438751142));
#30954=CARTESIAN_POINT('Ctrl Pts',(56.8288184694154,4.86226683676075,334.247427279006));
#30955=CARTESIAN_POINT('Ctrl Pts',(56.8210713261096,4.8375103039781,334.112488241539));
#30956=CARTESIAN_POINT('Ctrl Pts',(56.8133224410815,4.81274820540122,333.977518866912));
#30957=CARTESIAN_POINT('Ctrl Pts',(56.8055735560533,4.78233989782012,333.843622791111));
#30958=CARTESIAN_POINT('Ctrl Pts',(56.7978246710252,4.74641288146532,333.711299949111));
#30959=CARTESIAN_POINT('Ctrl Pts',(56.7900675612505,4.71044773180424,333.57883665828));
#30960=CARTESIAN_POINT('Ctrl Pts',(56.7823104514757,4.66895227481521,333.447950314738));
#30961=CARTESIAN_POINT('Ctrl Pts',(56.774553341701,4.62210397286131,333.31912584452));
#30962=CARTESIAN_POINT('Ctrl Pts',(56.7667920867748,4.57523063667273,333.190232534624));
#30963=CARTESIAN_POINT('Ctrl Pts',(56.7590308318486,4.52299890470561,333.063403654727));
#30964=CARTESIAN_POINT('Ctrl Pts',(56.7512695769224,4.46563388781244,332.939102854939));
#30965=CARTESIAN_POINT('Ctrl Pts',(56.7434959065178,4.40817710558753,332.81460321438));
#30966=CARTESIAN_POINT('Ctrl Pts',(56.7357222361131,4.34557080785631,332.692640083167));
#30967=CARTESIAN_POINT('Ctrl Pts',(56.7279485657084,4.27808586701096,332.573652049482));
#30968=CARTESIAN_POINT('Ctrl Pts',(56.7205367615314,4.21374236639908,332.460202937395));
#30969=CARTESIAN_POINT('Ctrl Pts',(56.7131249573545,4.14496435465852,332.349458419038));
#30970=CARTESIAN_POINT('Ctrl Pts',(56.7057131531776,4.07202150444447,332.241771595781));
#30971=CARTESIAN_POINT('Ctrl Pts',(56.6979380743991,3.99550350785452,332.128806720532));
#30972=CARTESIAN_POINT('Ctrl Pts',(56.6901629956207,3.91416027658614,332.018849862764));
#30973=CARTESIAN_POINT('Ctrl Pts',(56.6823879168423,3.82825592354718,331.912340749641));
#30974=CARTESIAN_POINT('Ctrl Pts',(56.6746224057933,3.74245728128369,331.805962702763));
#30975=CARTESIAN_POINT('Ctrl Pts',(56.6668568947443,3.65210892805783,331.703024260175));
#30976=CARTESIAN_POINT('Ctrl Pts',(56.6590913836953,3.55751870867872,331.603937029456));
#30977=CARTESIAN_POINT('Ctrl Pts',(56.6513335721731,3.46302227577733,331.504948044014));
#30978=CARTESIAN_POINT('Ctrl Pts',(56.6435757606508,3.3642926147085,331.409802952345));
#30979=CARTESIAN_POINT('Ctrl Pts',(56.6358179491286,3.26167813316202,331.318880765562));
#30980=CARTESIAN_POINT('Ctrl Pts',(56.6280659756056,3.15914087226707,331.228027000607));
#30981=CARTESIAN_POINT('Ctrl Pts',(56.6203140020826,3.05272490125626,331.141390073319));
#30982=CARTESIAN_POINT('Ctrl Pts',(56.6125620285596,2.94281555878699,331.059312287245));
#30983=CARTESIAN_POINT('Ctrl Pts',(56.604813338002,2.83295276298965,330.977269261161));
#30984=CARTESIAN_POINT('Ctrl Pts',(56.5970646474443,2.71959985077697,330.899781769459));
#30985=CARTESIAN_POINT('Ctrl Pts',(56.5893159568867,2.60317515389412,330.827151790366));
#30986=CARTESIAN_POINT('Ctrl Pts',(56.5815688785089,2.48677468014185,330.754536922546));
#30987=CARTESIAN_POINT('Ctrl Pts',(56.5738218001311,2.36730402438114,330.686777763845));
#30988=CARTESIAN_POINT('Ctrl Pts',(56.5660747217533,2.24521007141623,330.624132680518));
#30989=CARTESIAN_POINT('Ctrl Pts',(56.5583275784475,2.12311509518648,330.561487072165));
#30990=CARTESIAN_POINT('Ctrl Pts',(56.5505804351417,1.99839712566912,330.503955803113));
#30991=CARTESIAN_POINT('Ctrl Pts',(56.5428332918359,1.87152682984747,330.451750843713));
#30992=CARTESIAN_POINT('Ctrl Pts',(56.5350844068078,1.74462801088971,330.399534147531));
#30993=CARTESIAN_POINT('Ctrl Pts',(56.5273355217797,1.61557626414142,330.352646292538));
#30994=CARTESIAN_POINT('Ctrl Pts',(56.5195866367516,1.48486099327881,330.311250604571));
#30995=CARTESIAN_POINT('Ctrl Pts',(56.5118295269769,1.35400697987717,330.269810978793));
#30996=CARTESIAN_POINT('Ctrl Pts',(56.5040724172021,1.22148628846988,330.233875283094));
#30997=CARTESIAN_POINT('Ctrl Pts',(56.4963153074274,1.08780273877196,330.20355670689));
#30998=CARTESIAN_POINT('Ctrl Pts',(56.4885540525012,0.954047752859172,330.173221929408));
#30999=CARTESIAN_POINT('Ctrl Pts',(56.4807927975751,0.819129054755004,330.148510322783));
#31000=CARTESIAN_POINT('Ctrl Pts',(56.4730315426489,0.683558358126731,330.129483494173));
#31001=CARTESIAN_POINT('Ctrl Pts',(56.4652578722443,0.547770792566609,330.110426228838));
#31002=CARTESIAN_POINT('Ctrl Pts',(56.4574842018396,0.41132953350921,330.097071951704));
#31003=CARTESIAN_POINT('Ctrl Pts',(56.4497105314349,0.274749983709251,330.08943022563));
#31004=CARTESIAN_POINT('Ctrl Pts',(56.4422987272578,0.144528244811165,330.082144223744));
#31005=CARTESIAN_POINT('Ctrl Pts',(56.4348869230807,0.0141810880569334,
330.080050907729));
#31006=CARTESIAN_POINT('Ctrl Pts',(56.4274751189036,-0.115848620730662,
330.083114587508));
#31007=CARTESIAN_POINT('Ctrl Pts',(56.4197000401252,-0.252251472883883,
330.08632842736));
#31008=CARTESIAN_POINT('Ctrl Pts',(56.4119249613468,-0.38873603032035,330.095227720854));
#31009=CARTESIAN_POINT('Ctrl Pts',(56.4041498825684,-0.524789590437118,
330.109828331411));
#31010=CARTESIAN_POINT('Ctrl Pts',(56.3963843715194,-0.660675727986569,
330.124410974988));
#31011=CARTESIAN_POINT('Ctrl Pts',(56.3886188604704,-0.796131538572317,
330.144680934822));
#31012=CARTESIAN_POINT('Ctrl Pts',(56.3808533494214,-0.930644300109056,
330.170602082125));
#31013=CARTESIAN_POINT('Ctrl Pts',(56.3730955378992,-1.06502369185111,330.196497528535));
#31014=CARTESIAN_POINT('Ctrl Pts',(56.365337726377,-1.19846151397801,330.228032938307));
#31015=CARTESIAN_POINT('Ctrl Pts',(56.3575799148549,-1.33045050456621,330.26512043264));
#31016=CARTESIAN_POINT('Ctrl Pts',(56.3498279413318,-1.46234016925374,330.302180017459));
#31017=CARTESIAN_POINT('Ctrl Pts',(56.3420759678088,-1.59278279778895,330.344783265186));
#31018=CARTESIAN_POINT('Ctrl Pts',(56.3343239942858,-1.7212820109589,330.392791376414));
#31019=CARTESIAN_POINT('Ctrl Pts',(56.3265753037282,-1.84972680463568,330.440779156178));
#31020=CARTESIAN_POINT('Ctrl Pts',(56.3188266131706,-1.97622945451844,330.494167110345));
#31021=CARTESIAN_POINT('Ctrl Pts',(56.311077922613,-2.10030963736182,330.552766872571));
#31022=CARTESIAN_POINT('Ctrl Pts',(56.3033308442351,-2.22436400428681,330.611354442627));
#31023=CARTESIAN_POINT('Ctrl Pts',(56.2955837658573,-2.34599655347423,330.675151497058));
#31024=CARTESIAN_POINT('Ctrl Pts',(56.2878366874794,-2.46474818421698,330.743922057704));
#31025=CARTESIAN_POINT('Ctrl Pts',(56.2800895441736,-2.58350081021221,330.812693194713));
#31026=CARTESIAN_POINT('Ctrl Pts',(56.2723424008679,-2.6993721313554,330.886437725194));
#31027=CARTESIAN_POINT('Ctrl Pts',(56.2645952575621,-2.81192919234291,330.964874564558));
#31028=CARTESIAN_POINT('Ctrl Pts',(56.256846372534,-2.92451155854755,331.043329038189));
#31029=CARTESIAN_POINT('Ctrl Pts',(56.249097487506,-3.03377786127287,331.126477696467));
#31030=CARTESIAN_POINT('Ctrl Pts',(56.2413486024779,-3.13932591192704,331.21399737438));
#31031=CARTESIAN_POINT('Ctrl Pts',(56.2335914927032,-3.24498599237297,331.301609946583));
#31032=CARTESIAN_POINT('Ctrl Pts',(56.2258343829284,-3.34691963569661,331.39360255626));
#31033=CARTESIAN_POINT('Ctrl Pts',(56.2180772731537,-3.44475901274711,331.489612783951));
#31034=CARTESIAN_POINT('Ctrl Pts',(56.2103160182276,-3.5426506720322,331.585674316438));
#31035=CARTESIAN_POINT('Ctrl Pts',(56.2025547633014,-3.63644343841991,331.685757459741));
#31036=CARTESIAN_POINT('Ctrl Pts',(56.1947935083752,-3.7258085875077,331.789465242089));
#31037=CARTESIAN_POINT('Ctrl Pts',(56.1870198379706,-3.81531669171012,331.893338923091));
#31038=CARTESIAN_POINT('Ctrl Pts',(56.1792461675659,-3.90038278252682,332.000848523054));
#31039=CARTESIAN_POINT('Ctrl Pts',(56.1714724971613,-3.98071990434125,332.111565803817));
#31040=CARTESIAN_POINT('Ctrl Pts',(56.1640606929841,-4.05731731380821,332.217129168524));
#31041=CARTESIAN_POINT('Ctrl Pts',(56.1566488888069,-4.12961595374309,332.325608060064));
#31042=CARTESIAN_POINT('Ctrl Pts',(56.1492370846297,-4.1974061765844,332.43661074917));
#31043=CARTESIAN_POINT('Ctrl Pts',(56.1412198285504,-4.27073401461147,332.556680972664));
#31044=CARTESIAN_POINT('Ctrl Pts',(56.1332025724711,-4.33900642600092,332.680064084548));
#31045=CARTESIAN_POINT('Ctrl Pts',(56.1251853163918,-4.40192101234788,332.806310308282));
#31046=CARTESIAN_POINT('Ctrl Pts',(56.1171799294359,-4.46474245697842,332.932369631161));
#31047=CARTESIAN_POINT('Ctrl Pts',(56.10917454248,-4.52222171530947,333.061283306954));
#31048=CARTESIAN_POINT('Ctrl Pts',(56.1011691555242,-4.57410032287582,333.192573846939));
#31049=CARTESIAN_POINT('Ctrl Pts',(56.0931743527628,-4.62591033996967,333.323690803234));
#31050=CARTESIAN_POINT('Ctrl Pts',(56.0851795500014,-4.67213432462472,333.457178033807));
#31051=CARTESIAN_POINT('Ctrl Pts',(56.0771847472401,-4.71256030916059,333.59253476241));
#31052=CARTESIAN_POINT('Ctrl Pts',(56.069201958957,-4.75292554208981,333.727688078806));
#31053=CARTESIAN_POINT('Ctrl Pts',(56.0612191706739,-4.7875100435083,333.864704951177));
#31054=CARTESIAN_POINT('Ctrl Pts',(56.0532363823908,-4.8161506074193,334.003066507156));
#31055=CARTESIAN_POINT('Ctrl Pts',(56.0452607064753,-4.84476565365275,334.141304788132));
#31056=CARTESIAN_POINT('Ctrl Pts',(56.0372850305599,-4.86744723670225,334.280885017952));
#31057=CARTESIAN_POINT('Ctrl Pts',(56.0293093546443,-4.88408227987325,334.421274377681));
#31058=CARTESIAN_POINT('Ctrl Pts',(56.0213410202696,-4.90070201063064,334.561534510217));
#31059=CARTESIAN_POINT('Ctrl Pts',(56.0133726858949,-4.91128625380656,334.702601933746));
#31060=CARTESIAN_POINT('Ctrl Pts',(56.0054043515202,-4.91577326859276,334.843935159985));
#31061=CARTESIAN_POINT('Ctrl Pts',(56.0024483171769,-4.91743782848488,334.896365925434));
#31062=CARTESIAN_POINT('Ctrl Pts',(55.9994922828334,-4.91826379365925,334.94883319718));
#31063=CARTESIAN_POINT('Ctrl Pts',(55.9965362484901,-4.91824982577043,335.00130912533));
#31064=CARTESIAN_POINT('',(59.4965362854383,-4.92235223384019,335.000920754802));
#31065=CARTESIAN_POINT('Ctrl Pts',(59.4965362484901,-4.92614409942434,335.000922113078));
#31066=CARTESIAN_POINT('Ctrl Pts',(59.4937219976324,-4.9262713585574,335.050394967013));
#31067=CARTESIAN_POINT('Ctrl Pts',(59.39816173535,-4.90316042549208,336.730165617781));
#31068=CARTESIAN_POINT('Ctrl Pts',(59.209855461643,-2.99763204210603,339.983838982809));
#31069=CARTESIAN_POINT('Ctrl Pts',(58.9316174273691,2.56882582411236,340.217813982101));
#31070=CARTESIAN_POINT('Ctrl Pts',(58.6533793930951,5.77791014734984,335.663478104826));
#31071=CARTESIAN_POINT('Ctrl Pts',(58.3751413588212,3.68469161017836,330.500278163674));
#31072=CARTESIAN_POINT('Ctrl Pts',(58.0969033245472,-1.78991403169479,329.466406535932));
#31073=CARTESIAN_POINT('Ctrl Pts',(57.887368524017,-4.6757280257409,332.512021663937));
#31074=CARTESIAN_POINT('Ctrl Pts',(57.7705797349114,-4.92074476144685,334.570768816846));
#31075=CARTESIAN_POINT('Ctrl Pts',(57.7465369572303,-4.91693737480017,334.995484483173));
#31076=CARTESIAN_POINT('',(61.246536248442,-4.91824836367761,335.004011942491));
#31077=CARTESIAN_POINT('Ctrl Pts',(61.2465362484419,-4.91824836367761,335.004011942491));
#31078=CARTESIAN_POINT('Ctrl Pts',(61.2373935566682,-4.91811632314456,335.165880697366));
#31079=CARTESIAN_POINT('Ctrl Pts',(61.2282508648945,-4.9099893496518,335.327409458201));
#31080=CARTESIAN_POINT('Ctrl Pts',(61.2191081731208,-4.89399104746928,335.48788798898));
#31081=CARTESIAN_POINT('Ctrl Pts',(61.2099024893427,-4.87788251898293,335.649472196791));
#31082=CARTESIAN_POINT('Ctrl Pts',(61.2006968055647,-4.85379392770351,335.809991592536));
#31083=CARTESIAN_POINT('Ctrl Pts',(61.1914911217866,-4.82190030170716,335.968741731782));
#31084=CARTESIAN_POINT('Ctrl Pts',(61.1822161920626,-4.78976676911054,336.128686003242));
#31085=CARTESIAN_POINT('Ctrl Pts',(61.1729412623387,-4.74971040607306,336.286834244761));
#31086=CARTESIAN_POINT('Ctrl Pts',(61.1636663326148,-4.70195835134677,336.442487686152));
#31087=CARTESIAN_POINT('Ctrl Pts',(61.1616181222634,-4.6914131228975,336.476861099145));
#31088=CARTESIAN_POINT('Ctrl Pts',(61.159569911912,-4.68049277986775,336.511112932837));
#31089=CARTESIAN_POINT('Ctrl Pts',(61.1575217015606,-4.66920007739127,336.545235807179));
#31090=CARTESIAN_POINT('Ctrl Pts',(61.1497466227822,-4.62633258025302,336.674767442432));
#31091=CARTESIAN_POINT('Ctrl Pts',(61.1419715440037,-4.57800311475789,336.802718583922));
#31092=CARTESIAN_POINT('Ctrl Pts',(61.1341964652253,-4.52434608075795,336.928594204085));
#31093=CARTESIAN_POINT('Ctrl Pts',(61.1264309541762,-4.47075507515425,337.054314926284));
#31094=CARTESIAN_POINT('Ctrl Pts',(61.1186654431272,-4.4118496972396,337.177964852875));
#31095=CARTESIAN_POINT('Ctrl Pts',(61.1108999320782,-4.34781408305863,337.2990641056));
#31096=CARTESIAN_POINT('Ctrl Pts',(61.103142120556,-4.28384196037555,337.420043288062));
#31097=CARTESIAN_POINT('Ctrl Pts',(61.0953843090337,-4.21474990567511,337.538476486199));
#31098=CARTESIAN_POINT('Ctrl Pts',(61.0876264975115,-4.14076996092782,337.653904141671));
#31099=CARTESIAN_POINT('Ctrl Pts',(61.0798745239885,-4.06684568843509,337.769244934172));
#31100=CARTESIAN_POINT('Ctrl Pts',(61.0721225504655,-3.98804105742427,337.881584358183));
#31101=CARTESIAN_POINT('Ctrl Pts',(61.0643705769425,-3.90463364052436,337.990488119987));
#31102=CARTESIAN_POINT('Ctrl Pts',(61.0566218863849,-3.82126154671502,338.099345760984));
#31103=CARTESIAN_POINT('Ctrl Pts',(61.0488731958272,-3.73329078117446,338.204770324002));
#31104=CARTESIAN_POINT('Ctrl Pts',(61.0411245052696,-3.64104164318245,338.306357333246));
#31105=CARTESIAN_POINT('Ctrl Pts',(61.0333774268918,-3.54881169839407,338.407923206465));
#31106=CARTESIAN_POINT('Ctrl Pts',(61.0256303485139,-3.45230541433311,338.505652824865));
#31107=CARTESIAN_POINT('Ctrl Pts',(61.0178832701361,-3.35188243959219,338.599175902016));
#31108=CARTESIAN_POINT('Ctrl Pts',(61.0101361268303,-3.25145862321008,338.692699762981));
#31109=CARTESIAN_POINT('Ctrl Pts',(61.0023889835245,-3.14711833671667,338.78201674599));
#31110=CARTESIAN_POINT('Ctrl Pts',(60.9946418402186,-3.03925674544342,338.866794731787));
#31111=CARTESIAN_POINT('Ctrl Pts',(60.9868929551905,-2.93137090459449,338.951591777475));
#31112=CARTESIAN_POINT('Ctrl Pts',(60.9791440701625,-2.81996249089327,339.031847553848));
#31113=CARTESIAN_POINT('Ctrl Pts',(60.9713951851344,-2.70545794384329,339.107271646312));
#31114=CARTESIAN_POINT('Ctrl Pts',(60.9636380753596,-2.59083186048403,339.182775794686));
#31115=CARTESIAN_POINT('Ctrl Pts',(60.9558809655849,-2.4731034060855,339.253437799337));
#31116=CARTESIAN_POINT('Ctrl Pts',(60.9481238558101,-2.35272654315668,339.31901156234));
#31117=CARTESIAN_POINT('Ctrl Pts',(60.940362600884,-2.23228535468121,339.384620365865));
#31118=CARTESIAN_POINT('Ctrl Pts',(60.9326013459578,-2.10919328831053,339.445135337539));
#31119=CARTESIAN_POINT('Ctrl Pts',(60.9248400910316,-1.98392594759599,339.50035786321));
#31120=CARTESIAN_POINT('Ctrl Pts',(60.917066420627,-1.85845821996083,339.555668726925));
#31121=CARTESIAN_POINT('Ctrl Pts',(60.9092927502223,-1.73080862859112,339.605670084048));
#31122=CARTESIAN_POINT('Ctrl Pts',(60.9015190798176,-1.6014704979069,339.650212393734));
#31123=CARTESIAN_POINT('Ctrl Pts',(60.8941072756407,-1.47815308832491,339.692681248186));
#31124=CARTESIAN_POINT('Ctrl Pts',(60.8866954714637,-1.35330108031076,339.730187772153));
#31125=CARTESIAN_POINT('Ctrl Pts',(60.8792836672867,-1.22735032410398,339.76264571897));
#31126=CARTESIAN_POINT('Ctrl Pts',(60.8715085885083,-1.09522634614551,339.796694526447));
#31127=CARTESIAN_POINT('Ctrl Pts',(60.8637335097299,-0.961475654625873,
339.825294952343));
#31128=CARTESIAN_POINT('Ctrl Pts',(60.8559584309514,-0.826587260254591,
339.848292128542));
#31129=CARTESIAN_POINT('Ctrl Pts',(60.8481929199024,-0.691864854639906,
339.871261005252));
#31130=CARTESIAN_POINT('Ctrl Pts',(60.8404274088534,-0.556007913434547,
339.888640286582));
#31131=CARTESIAN_POINT('Ctrl Pts',(60.8326618978044,-0.419519623083472,
339.9003251268));
#31132=CARTESIAN_POINT('Ctrl Pts',(60.8249040862822,-0.283166661269655,
339.911998381465));
#31133=CARTESIAN_POINT('Ctrl Pts',(60.81714627476,-0.146183982995693,339.91798839786));
#31134=CARTESIAN_POINT('Ctrl Pts',(60.8093884632378,-0.00908361189721485,
339.918241611643));
#31135=CARTESIAN_POINT('Ctrl Pts',(60.8016364897148,0.127913586824123,339.918494634874));
#31136=CARTESIAN_POINT('Ctrl Pts',(60.7938845161918,0.265027912780756,339.913019447802));
#31137=CARTESIAN_POINT('Ctrl Pts',(60.7861325426688,0.401743948642575,339.90181444592));
#31138=CARTESIAN_POINT('Ctrl Pts',(60.7783838521111,0.538402085182131,339.890614189363));
#31139=CARTESIAN_POINT('Ctrl Pts',(60.7706351615535,0.674661878354404,339.873688976156));
#31140=CARTESIAN_POINT('Ctrl Pts',(60.7628864709959,0.810009863513417,339.851089267733));
#31141=CARTESIAN_POINT('Ctrl Pts',(60.755139392618,0.945329688393576,339.828494261368));
#31142=CARTESIAN_POINT('Ctrl Pts',(60.7473923142402,1.07973769731095,339.80022717247));
#31143=CARTESIAN_POINT('Ctrl Pts',(60.7396452358624,1.21272788201621,339.76639005398));
#31144=CARTESIAN_POINT('Ctrl Pts',(60.7318980925566,1.34571918130723,339.732552651902));
#31145=CARTESIAN_POINT('Ctrl Pts',(60.7241509492508,1.4772922538798,339.693145223501));
#31146=CARTESIAN_POINT('Ctrl Pts',(60.716403805945,1.60695396693021,339.648320342948));
#31147=CARTESIAN_POINT('Ctrl Pts',(60.7086549209169,1.73664483068643,339.60348538481));
#31148=CARTESIAN_POINT('Ctrl Pts',(60.7009060358888,1.8644231104876,339.553230678606));
#31149=CARTESIAN_POINT('Ctrl Pts',(60.6931571508607,1.9898138196204,339.49775766641));
#31150=CARTESIAN_POINT('Ctrl Pts',(60.685400041086,2.11533761974757,339.442225774585));
#31151=CARTESIAN_POINT('Ctrl Pts',(60.6776429313112,2.23846842889919,339.381464670957));
#31152=CARTESIAN_POINT('Ctrl Pts',(60.6698858215365,2.35875363291676,339.315722924575));
#31153=CARTESIAN_POINT('Ctrl Pts',(60.6621245666103,2.47910311350138,339.249946047906));
#31154=CARTESIAN_POINT('Ctrl Pts',(60.6543633116841,2.59660362434685,339.179183426762));
#31155=CARTESIAN_POINT('Ctrl Pts',(60.646602056758,2.71083077020372,339.103727524802));
#31156=CARTESIAN_POINT('Ctrl Pts',(60.6388283863533,2.82524064226742,339.02815091799));
#31157=CARTESIAN_POINT('Ctrl Pts',(60.6310547159486,2.93636636862656,338.947866256739));
#31158=CARTESIAN_POINT('Ctrl Pts',(60.623281045544,3.0438152310433,338.863207462947));
#31159=CARTESIAN_POINT('Ctrl Pts',(60.6158692413669,3.14626232306398,338.782489556373));
#31160=CARTESIAN_POINT('Ctrl Pts',(60.6084574371898,3.24536694477937,338.697795771474));
#31161=CARTESIAN_POINT('Ctrl Pts',(60.6010456330127,3.3408207059551,338.609445950996));
#31162=CARTESIAN_POINT('Ctrl Pts',(60.5932705542342,3.44095294030791,338.516765842636));
#31163=CARTESIAN_POINT('Ctrl Pts',(60.5854954754558,3.53738382240136,338.419769364235));
#31164=CARTESIAN_POINT('Ctrl Pts',(60.5777203966774,3.62971848857881,338.31878392731));
#31165=CARTESIAN_POINT('Ctrl Pts',(60.5699548856283,3.72193953107127,338.217922759393));
#31166=CARTESIAN_POINT('Ctrl Pts',(60.5621893745793,3.81007412586831,338.113082685504));
#31167=CARTESIAN_POINT('Ctrl Pts',(60.5544238635303,3.89376180289814,338.004630107816));
#31168=CARTESIAN_POINT('Ctrl Pts',(60.5466660520081,3.97736650335248,337.896285061174));
#31169=CARTESIAN_POINT('Ctrl Pts',(60.5389082404859,4.05653282320891,337.784334946195));
#31170=CARTESIAN_POINT('Ctrl Pts',(60.5311504289637,4.13093863369961,337.669181347737));
#31171=CARTESIAN_POINT('Ctrl Pts',(60.5233984554407,4.20528845145833,337.554114406014));
#31172=CARTESIAN_POINT('Ctrl Pts',(60.5156464819177,4.27488467923452,337.43584910622));
#31173=CARTESIAN_POINT('Ctrl Pts',(60.5078945083947,4.33944704587327,337.314818005495));
#31174=CARTESIAN_POINT('Ctrl Pts',(60.5001458178371,4.40398207031145,337.193838161512));
#31175=CARTESIAN_POINT('Ctrl Pts',(60.4923971272795,4.46348729011247,337.070095190423));
#31176=CARTESIAN_POINT('Ctrl Pts',(60.4846484367219,4.51772727419102,336.944048183181));
#31177=CARTESIAN_POINT('Ctrl Pts',(60.476901358344,4.57195597318787,336.818027401072));
#31178=CARTESIAN_POINT('Ctrl Pts',(60.4691542799662,4.62092146103723,336.689703895137));
#31179=CARTESIAN_POINT('Ctrl Pts',(60.4614072015883,4.66443572613481,336.559558405209));
#31180=CARTESIAN_POINT('Ctrl Pts',(60.4536600582825,4.70795035592381,336.429411824536));
#31181=CARTESIAN_POINT('Ctrl Pts',(60.4459129149767,4.74601354789115,336.297443600116));
#31182=CARTESIAN_POINT('Ctrl Pts',(60.4381657716709,4.7784867424562,336.164150984482));
#31183=CARTESIAN_POINT('Ctrl Pts',(60.4304168866428,4.8109672376848,336.030828401838));
#31184=CARTESIAN_POINT('Ctrl Pts',(60.4226680016147,4.83785514221687,335.896181215182));
#31185=CARTESIAN_POINT('Ctrl Pts',(60.4149191165866,4.85906281042534,335.760717862838));
#31186=CARTESIAN_POINT('Ctrl Pts',(60.4071620068119,4.88029298867198,335.625110728293));
#31187=CARTESIAN_POINT('Ctrl Pts',(60.3994048970371,4.89583082642603,335.488686084352));
#31188=CARTESIAN_POINT('Ctrl Pts',(60.3916477872624,4.90564041521214,335.351959058894));
#31189=CARTESIAN_POINT('Ctrl Pts',(60.3838865323362,4.91545524592883,335.215158970884));
#31190=CARTESIAN_POINT('Ctrl Pts',(60.3761252774101,4.91953571675091,335.078056569892));
#31191=CARTESIAN_POINT('Ctrl Pts',(60.3683640224839,4.91789810198718,334.941167007802));
#31192=CARTESIAN_POINT('Ctrl Pts',(60.3605903520792,4.91625786757352,334.804058467026));
#31193=CARTESIAN_POINT('Ctrl Pts',(60.3528166816745,4.90888129005536,334.667163836031));
#31194=CARTESIAN_POINT('Ctrl Pts',(60.3450430112699,4.89583664910739,334.530994064263));
#31195=CARTESIAN_POINT('Ctrl Pts',(60.3376312070928,4.88339923933396,334.401163028131));
#31196=CARTESIAN_POINT('Ctrl Pts',(60.3302194029158,4.86580962618219,334.27199117069));
#31197=CARTESIAN_POINT('Ctrl Pts',(60.3228075987387,4.84316988458913,334.143910909129));
#31198=CARTESIAN_POINT('Ctrl Pts',(60.3150325199603,4.81942050182019,334.009553052417));
#31199=CARTESIAN_POINT('Ctrl Pts',(60.3072574411819,4.7900383773079,333.875971906282));
#31200=CARTESIAN_POINT('Ctrl Pts',(60.2994823624034,4.75508515499803,333.743676701156));
#31201=CARTESIAN_POINT('Ctrl Pts',(60.2917168513544,4.72017494485344,333.611544293703));
#31202=CARTESIAN_POINT('Ctrl Pts',(60.2839513403054,4.67970737646155,333.480695052965));
#31203=CARTESIAN_POINT('Ctrl Pts',(60.2761858292564,4.6337954941881,333.351630387158));
#31204=CARTESIAN_POINT('Ctrl Pts',(60.2684280177342,4.58792913367964,333.222693689342));
#31205=CARTESIAN_POINT('Ctrl Pts',(60.260670206212,4.5366293318795,333.095538411124));
#31206=CARTESIAN_POINT('Ctrl Pts',(60.2529123946898,4.48005946770334,332.970652758067));
#31207=CARTESIAN_POINT('Ctrl Pts',(60.2451604211668,4.42353217414386,332.845861085424));
#31208=CARTESIAN_POINT('Ctrl Pts',(60.2374084476438,4.36174287274813,332.723335992936));
#31209=CARTESIAN_POINT('Ctrl Pts',(60.2296564741208,4.29490363923846,332.603547248086));
#31210=CARTESIAN_POINT('Ctrl Pts',(60.2219077835632,4.22809271218391,332.48380923384));
#31211=CARTESIAN_POINT('Ctrl Pts',(60.2141590930056,4.15623629669805,332.366805602995));
#31212=CARTESIAN_POINT('Ctrl Pts',(60.2064104024479,4.07959304688827,332.25298277503));
#31213=CARTESIAN_POINT('Ctrl Pts',(60.1986633240701,4.00296574334676,332.139183628855));
#31214=CARTESIAN_POINT('Ctrl Pts',(60.1909162456923,3.92155380465824,332.028564293227));
#31215=CARTESIAN_POINT('Ctrl Pts',(60.1831691673145,3.83565975133767,331.921543027023));
#31216=CARTESIAN_POINT('Ctrl Pts',(60.1754220240087,3.74976497814225,331.814520863879));
#31217=CARTESIAN_POINT('Ctrl Pts',(60.1676748807029,3.65938826004781,331.711097135142));
#31218=CARTESIAN_POINT('Ctrl Pts',(60.1599277373971,3.5648727647788,331.611657450399));
#31219=CARTESIAN_POINT('Ctrl Pts',(60.152178852369,3.47033602041984,331.512195409503));
#31220=CARTESIAN_POINT('Ctrl Pts',(60.1444299673409,3.37165891655857,331.4167194782));
#31221=CARTESIAN_POINT('Ctrl Pts',(60.1366810823128,3.26922157975248,331.325578504719));
#31222=CARTESIAN_POINT('Ctrl Pts',(60.128923972538,3.16667551489865,331.234340793268));
#31223=CARTESIAN_POINT('Ctrl Pts',(60.1211668627633,3.06036153688643,331.147447491134));
#31224=CARTESIAN_POINT('Ctrl Pts',(60.1134097529886,2.95069339560144,331.065207559775));
#31225=CARTESIAN_POINT('Ctrl Pts',(60.1056484980624,2.84096665116833,330.982923682026));
#31226=CARTESIAN_POINT('Ctrl Pts',(60.0978872431363,2.72788249412141,330.905298350947));
#31227=CARTESIAN_POINT('Ctrl Pts',(60.0901259882101,2.61188293363476,330.832596659371));
#31228=CARTESIAN_POINT('Ctrl Pts',(60.0823523178054,2.4956978116555,330.759778668781));
#31229=CARTESIAN_POINT('Ctrl Pts',(60.0745786474008,2.37658830657052,330.691900250345));
#31230=CARTESIAN_POINT('Ctrl Pts',(60.0668049769961,2.25502103671737,330.62918049029));
#31231=CARTESIAN_POINT('Ctrl Pts',(60.059393172819,2.13911275252312,330.569380350154));
#31232=CARTESIAN_POINT('Ctrl Pts',(60.051981368642,2.02097063287131,330.51426952717));
#31233=CARTESIAN_POINT('Ctrl Pts',(60.0445695644649,1.90101354520732,330.463996190099));
#31234=CARTESIAN_POINT('Ctrl Pts',(60.0367944856864,1.77517700334329,330.411258807021));
#31235=CARTESIAN_POINT('Ctrl Pts',(60.029019406908,1.64694541421068,330.363678439306));
#31236=CARTESIAN_POINT('Ctrl Pts',(60.0212443281296,1.51678035961847,330.321478823049));
#31237=CARTESIAN_POINT('Ctrl Pts',(60.0134788170806,1.38677548141265,330.279331136107));
#31238=CARTESIAN_POINT('Ctrl Pts',(60.0057133060316,1.25484224004473,330.242551145415));
#31239=CARTESIAN_POINT('Ctrl Pts',(59.9979477949825,1.12146345517206,330.211315130308));
#31240=CARTESIAN_POINT('Ctrl Pts',(59.9901899834603,0.988216915753007,330.180110085802));
#31241=CARTESIAN_POINT('Ctrl Pts',(59.9824321719381,0.853528063224444,330.154438166357));
#31242=CARTESIAN_POINT('Ctrl Pts',(59.9746743604159,0.717895853766025,330.134426179201));
#31243=CARTESIAN_POINT('Ctrl Pts',(59.9669223868929,0.582365711846368,330.1144292517));
#31244=CARTESIAN_POINT('Ctrl Pts',(59.9591704133699,0.445894011160946,330.100083835427));
#31245=CARTESIAN_POINT('Ctrl Pts',(59.9514184398469,0.308990555549207,330.091465809523));
#31246=CARTESIAN_POINT('Ctrl Pts',(59.9436697492893,0.172145078632198,330.082851433358));
#31247=CARTESIAN_POINT('Ctrl Pts',(59.9359210587316,0.0348685997518534,
330.079959647812));
#31248=CARTESIAN_POINT('Ctrl Pts',(59.928172368174,-0.10232350484836,330.082814528325));
#31249=CARTESIAN_POINT('Ctrl Pts',(59.9204252897962,-0.239487065485361,
330.085668814856));
#31250=CARTESIAN_POINT('Ctrl Pts',(59.9126782114184,-0.376565896215581,
330.094267381102));
#31251=CARTESIAN_POINT('Ctrl Pts',(59.9049311330405,-0.513044563016202,
330.108582174987));
#31252=CARTESIAN_POINT('Ctrl Pts',(59.8971839897347,-0.64952437363941,330.122897088843));
#31253=CARTESIAN_POINT('Ctrl Pts',(59.8894368464289,-0.785403621558577,
330.14292828512));
#31254=CARTESIAN_POINT('Ctrl Pts',(59.8816897031231,-0.92017233169974,330.168595862229));
#31255=CARTESIAN_POINT('Ctrl Pts',(59.873940818095,-1.05497134070807,330.194269209954));
#31256=CARTESIAN_POINT('Ctrl Pts',(59.8661919330669,-1.18865893122083,330.225581386939));
#31257=CARTESIAN_POINT('Ctrl Pts',(59.8584430480389,-1.32073604102711,330.262401518445));
#31258=CARTESIAN_POINT('Ctrl Pts',(59.8506859382641,-1.45295333884254,330.29926073122));
#31259=CARTESIAN_POINT('Ctrl Pts',(59.8429288284894,-1.583556364191,330.341639471718));
#31260=CARTESIAN_POINT('Ctrl Pts',(59.8351717187147,-1.71206140098901,330.389357005607));
#31261=CARTESIAN_POINT('Ctrl Pts',(59.8274104637885,-1.84063510676971,330.43710003822));
#31262=CARTESIAN_POINT('Ctrl Pts',(59.8196492088623,-1.96710822988306,330.490187397639));
#31263=CARTESIAN_POINT('Ctrl Pts',(59.8118879539362,-2.09101865158471,330.54839084586));
#31264=CARTESIAN_POINT('Ctrl Pts',(59.8041142835315,-2.21512728957886,330.60668740063));
#31265=CARTESIAN_POINT('Ctrl Pts',(59.7963406131268,-2.33666468746766,330.670116217467));
#31266=CARTESIAN_POINT('Ctrl Pts',(59.7885669427222,-2.45519409701178,330.738403467185));
#31267=CARTESIAN_POINT('Ctrl Pts',(59.7811551385451,-2.5682059340255,330.803511929));
#31268=CARTESIAN_POINT('Ctrl Pts',(59.773743334368,-2.67848328074788,330.873036529292));
#31269=CARTESIAN_POINT('Ctrl Pts',(59.7663315301909,-2.78567486569737,330.946705216109));
#31270=CARTESIAN_POINT('Ctrl Pts',(59.7585951336949,-2.89756079554421,331.023600147076));
#31271=CARTESIAN_POINT('Ctrl Pts',(59.7508587371989,-3.00644595196727,331.105258833066));
#31272=CARTESIAN_POINT('Ctrl Pts',(59.743122340703,-3.11189487609635,331.191418460552));
#31273=CARTESIAN_POINT('Ctrl Pts',(59.7353954868895,-3.21721373119349,331.277471811948));
#31274=CARTESIAN_POINT('Ctrl Pts',(59.7276686330761,-3.31910448276863,331.368014812905));
#31275=CARTESIAN_POINT('Ctrl Pts',(59.7199417792626,-3.41715987418023,331.462740968378));
#31276=CARTESIAN_POINT('Ctrl Pts',(59.7122225605611,-3.51511837442402,331.557373522391));
#31277=CARTESIAN_POINT('Ctrl Pts',(59.7045033418596,-3.60924877267888,331.65618073379));
#31278=CARTESIAN_POINT('Ctrl Pts',(59.6967841231581,-3.69917653089978,331.758815639964));
#31279=CARTESIAN_POINT('Ctrl Pts',(59.6890706390703,-3.78903748171775,331.861374298586));
#31280=CARTESIAN_POINT('Ctrl Pts',(59.6813571549825,-3.87470174650037,331.967754696837));
#31281=CARTESIAN_POINT('Ctrl Pts',(59.6736436708947,-3.95583164723709,332.077573090526));
#31282=CARTESIAN_POINT('Ctrl Pts',(59.6659333188321,-4.03692860554529,332.187346892954));
#31283=CARTESIAN_POINT('Ctrl Pts',(59.6582229667696,-4.11349462648461,332.300555597711));
#31284=CARTESIAN_POINT('Ctrl Pts',(59.650512614707,-4.18523252934497,332.416782677007));
#31285=CARTESIAN_POINT('Ctrl Pts',(59.6428037123741,-4.25695694377249,332.532987902846));
#31286=CARTESIAN_POINT('Ctrl Pts',(59.6350948100412,-4.32385483805942,332.65221003839));
#31287=CARTESIAN_POINT('Ctrl Pts',(59.6273859077083,-4.38567282591597,332.774004284253));
#31288=CARTESIAN_POINT('Ctrl Pts',(59.6196767431305,-4.44749291672514,332.89580267337));
#31289=CARTESIAN_POINT('Ctrl Pts',(59.6119675785526,-4.5042325784646,333.020172994421));
#31290=CARTESIAN_POINT('Ctrl Pts',(59.6042584139747,-4.55568499706754,333.14664701959));
#31291=CARTESIAN_POINT('Ctrl Pts',(59.5965472753277,-4.60715059098092,333.273153430692));
#31292=CARTESIAN_POINT('Ctrl Pts',(59.5888361366806,-4.65332609961916,333.401764251546));
#31293=CARTESIAN_POINT('Ctrl Pts',(59.5811249980335,-4.69405350941549,333.531992945097));
#31294=CARTESIAN_POINT('Ctrl Pts',(59.5734057227792,-4.73482389379036,333.662359052819));
#31295=CARTESIAN_POINT('Ctrl Pts',(59.565686447525,-4.77013458171241,333.794346064602));
#31296=CARTESIAN_POINT('Ctrl Pts',(59.5579671722708,-4.79987784009613,333.927453598834));
#31297=CARTESIAN_POINT('Ctrl Pts',(59.5502434732637,-4.82963814371007,334.060637414169));
#31298=CARTESIAN_POINT('Ctrl Pts',(59.5425197742566,-4.85382459290499,334.194942642628));
#31299=CARTESIAN_POINT('Ctrl Pts',(59.5347960752495,-4.8723810982895,334.329861584797));
#31300=CARTESIAN_POINT('Ctrl Pts',(59.5270608342684,-4.89096533374258,334.464982144212));
#31301=CARTESIAN_POINT('Ctrl Pts',(59.5193255932873,-4.90390278545122,334.600717856209));
#31302=CARTESIAN_POINT('Ctrl Pts',(59.5115903523062,-4.91118941666391,334.736558211082));
#31303=CARTESIAN_POINT('Ctrl Pts',(59.5065723433413,-4.91591640330058,334.824680626429));
#31304=CARTESIAN_POINT('Ctrl Pts',(59.5015543343764,-4.91826637593461,334.912847083949));
#31305=CARTESIAN_POINT('Ctrl Pts',(59.4965363254115,-4.91824991408677,335.000919285319));
#31306=CARTESIAN_POINT('',(62.9965362485424,-4.91824921808336,334.997226676644));
#31307=CARTESIAN_POINT('Ctrl Pts',(62.99653624849,-4.91824921808388,334.997226677573));
#31308=CARTESIAN_POINT('Ctrl Pts',(62.9887031285403,-4.91832755861146,335.136156877207));
#31309=CARTESIAN_POINT('Ctrl Pts',(62.9808700085906,-4.91251482706172,335.275093926432));
#31310=CARTESIAN_POINT('Ctrl Pts',(62.9730368886409,-4.90083586450775,335.413510449269));
#31311=CARTESIAN_POINT('Ctrl Pts',(62.9652022573993,-4.88915464865987,335.551953677655));
#31312=CARTESIAN_POINT('Ctrl Pts',(62.9573676261577,-4.87160497907927,335.6898758022));
#31313=CARTESIAN_POINT('Ctrl Pts',(62.9495329949161,-4.84826359170246,335.826754623738));
#31314=CARTESIAN_POINT('Ctrl Pts',(62.9416953021712,-4.82491308331758,335.963686932793));
#31315=CARTESIAN_POINT('Ctrl Pts',(62.9338576094262,-4.79576641330961,336.099574753729));
#31316=CARTESIAN_POINT('Ctrl Pts',(62.9260199166813,-4.76095139074702,336.233906364942));
#31317=CARTESIAN_POINT('Ctrl Pts',(62.9181776104982,-4.7261158752969,336.368317046694));
#31318=CARTESIAN_POINT('Ctrl Pts',(62.9103353043151,-4.68560545705694,336.501169328344));
#31319=CARTESIAN_POINT('Ctrl Pts',(62.9024929981319,-4.63959764255931,336.631967149687));
#31320=CARTESIAN_POINT('Ctrl Pts',(62.8946398519426,-4.59352623388616,336.76294576596));
#31321=CARTESIAN_POINT('Ctrl Pts',(62.8867867057531,-4.54194238104062,336.891863894192));
#31322=CARTESIAN_POINT('Ctrl Pts',(62.8789335595638,-4.48507179021934,337.018245302008));
#31323=CARTESIAN_POINT('Ctrl Pts',(62.8710739677352,-4.42815452163348,337.144730440092));
#31324=CARTESIAN_POINT('Ctrl Pts',(62.8632143759067,-4.36594203687394,337.268674371339));
#31325=CARTESIAN_POINT('Ctrl Pts',(62.8553547840781,-4.29870536434282,337.389626592811));
#31326=CARTESIAN_POINT('Ctrl Pts',(62.8474829775086,-4.23136419802172,337.510766788429));
#31327=CARTESIAN_POINT('Ctrl Pts',(62.8396111709391,-4.15898345072758,337.628905669596));
#31328=CARTESIAN_POINT('Ctrl Pts',(62.8317393643696,-4.0818770102074,337.743622265553));
#31329=CARTESIAN_POINT('Ctrl Pts',(62.8301428786478,-4.06623900763951,337.766888005874));
#31330=CARTESIAN_POINT('Ctrl Pts',(62.828546392926,-4.05040675680743,337.790013092481));
#31331=CARTESIAN_POINT('Ctrl Pts',(62.8269499072042,-4.03438307029467,337.812994188515));
#31332=CARTESIAN_POINT('Ctrl Pts',(62.8191748284258,-3.95634577672058,337.924914908911));
#31333=CARTESIAN_POINT('Ctrl Pts',(62.8113997496473,-3.87352433058407,338.033762692091));
#31334=CARTESIAN_POINT('Ctrl Pts',(62.8036246708689,-3.78618876188953,338.13910141949));
#31335=CARTESIAN_POINT('Ctrl Pts',(62.7958591598199,-3.69896066517238,338.244310520878));
#31336=CARTESIAN_POINT('Ctrl Pts',(62.7880936487709,-3.60722974567853,338.34601886027));
#31337=CARTESIAN_POINT('Ctrl Pts',(62.7803281377219,-3.51130938139486,338.443819026986));
#31338=CARTESIAN_POINT('Ctrl Pts',(62.7725703261997,-3.41548412243165,338.541522224551));
#31339=CARTESIAN_POINT('Ctrl Pts',(62.7648125146775,-3.31547795700033,338.635324683576));
#31340=CARTESIAN_POINT('Ctrl Pts',(62.7570547031553,-3.21164438185126,338.724852134921));
#31341=CARTESIAN_POINT('Ctrl Pts',(62.7493027296323,-3.10788894476045,338.814312214019));
#31342=CARTESIAN_POINT('Ctrl Pts',(62.7415507561093,-3.00031212578102,338.899503434659));
#31343=CARTESIAN_POINT('Ctrl Pts',(62.7337987825863,-2.88930385329977,338.980088730896));
#31344=CARTESIAN_POINT('Ctrl Pts',(62.7260500920286,-2.77834259288751,339.060639899213));
#31345=CARTESIAN_POINT('Ctrl Pts',(62.7183014014711,-2.66395308498706,339.136588793607));
#31346=CARTESIAN_POINT('Ctrl Pts',(62.7105527109134,-2.54655770322131,339.207639115545));
#31347=CARTESIAN_POINT('Ctrl Pts',(62.7028056325356,-2.42918674654533,339.27867465487));
#31348=CARTESIAN_POINT('Ctrl Pts',(62.6950585541577,-2.30881149415232,339.344813446718));
#31349=CARTESIAN_POINT('Ctrl Pts',(62.6873114757799,-2.18588228087157,339.40580318633));
#31350=CARTESIAN_POINT('Ctrl Pts',(62.6795643324741,-2.0629520373257,339.466793437093));
#31351=CARTESIAN_POINT('Ctrl Pts',(62.6718171891683,-1.93746814034687,339.522634375824));
#31352=CARTESIAN_POINT('Ctrl Pts',(62.6640700458625,-1.80990407791222,339.573120410754));
#31353=CARTESIAN_POINT('Ctrl Pts',(62.6563211608344,-1.68231133636815,339.623617796016));
#31354=CARTESIAN_POINT('Ctrl Pts',(62.6485722758063,-1.55263786214078,339.668757738046));
#31355=CARTESIAN_POINT('Ctrl Pts',(62.6408233907782,-1.42137522094821,339.708383538304));
#31356=CARTESIAN_POINT('Ctrl Pts',(62.6330662810034,-1.28997325623171,339.748051397796));
#31357=CARTESIAN_POINT('Ctrl Pts',(62.6253091712287,-1.15697912987852,339.782193310924));
#31358=CARTESIAN_POINT('Ctrl Pts',(62.617552061454,-1.02289814493059,339.810702905771));
#31359=CARTESIAN_POINT('Ctrl Pts',(62.6097908065278,-0.888745511391657,
339.839227735234));
#31360=CARTESIAN_POINT('Ctrl Pts',(62.6020295516016,-0.753505247195832,
339.86211418407));
#31361=CARTESIAN_POINT('Ctrl Pts',(62.5942682966754,-0.617689851683025,
339.879307564566));
#31362=CARTESIAN_POINT('Ctrl Pts',(62.5864946262708,-0.48165719579944,339.896528448866));
#31363=CARTESIAN_POINT('Ctrl Pts',(62.5787209558661,-0.345047959820318,
339.908038033402));
#31364=CARTESIAN_POINT('Ctrl Pts',(62.5709472854614,-0.20837762865966,339.913833719854));
#31365=CARTESIAN_POINT('Ctrl Pts',(62.5635354812844,-0.0780693342963419,
339.919359615707));
#31366=CARTESIAN_POINT('Ctrl Pts',(62.5561236771073,0.0522942074957861,
339.919691605138));
#31367=CARTESIAN_POINT('Ctrl Pts',(62.5487118729303,0.182270653531195,339.914871358577));
#31368=CARTESIAN_POINT('Ctrl Pts',(62.5409367941519,0.318617632367615,339.909814857374));
#31369=CARTESIAN_POINT('Ctrl Pts',(62.5331617153734,0.454969492207677,339.899072317563));
#31370=CARTESIAN_POINT('Ctrl Pts',(62.525386636595,0.590813362915036,339.882634804355));
#31371=CARTESIAN_POINT('Ctrl Pts',(62.517621125546,0.726490069091153,339.866217518554));
#31372=CARTESIAN_POINT('Ctrl Pts',(62.509855614497,0.861659645595877,339.844119249827));
#31373=CARTESIAN_POINT('Ctrl Pts',(62.502090103448,0.995809905285056,339.816383051112));
#31374=CARTESIAN_POINT('Ctrl Pts',(62.4943322919258,1.12982715460091,339.788674352918));
#31375=CARTESIAN_POINT('Ctrl Pts',(62.4865744804036,1.26282671805026,339.755338927832));
#31376=CARTESIAN_POINT('Ctrl Pts',(62.4788166688814,1.39430256735267,339.716471500303));
#31377=CARTESIAN_POINT('Ctrl Pts',(62.4710646953584,1.52567947690887,339.677633321747));
#31378=CARTESIAN_POINT('Ctrl Pts',(62.4633127218354,1.65553458132659,339.633271537376));
#31379=CARTESIAN_POINT('Ctrl Pts',(62.4555607483124,1.78337342203687,339.583531640566));
#31380=CARTESIAN_POINT('Ctrl Pts',(62.4478120577548,1.91115812292272,339.533812808632));
#31381=CARTESIAN_POINT('Ctrl Pts',(62.4400633671972,2.03692789491125,339.478720535749));
#31382=CARTESIAN_POINT('Ctrl Pts',(62.4323146766396,2.16020500364008,339.418449660769));
#31383=CARTESIAN_POINT('Ctrl Pts',(62.4245675982617,2.28345646353665,339.358191325648));
#31384=CARTESIAN_POINT('Ctrl Pts',(62.4168205198839,2.40421594081165,339.292756703129));
#31385=CARTESIAN_POINT('Ctrl Pts',(62.4090734415061,2.52202756499258,339.222387952796));
#31386=CARTESIAN_POINT('Ctrl Pts',(62.4013262982003,2.63984017654832,339.152018612705));
#31387=CARTESIAN_POINT('Ctrl Pts',(62.3935791548944,2.75470455016115,339.076715262754));
#31388=CARTESIAN_POINT('Ctrl Pts',(62.3858320115886,2.86619156781367,338.996764811581));
#31389=CARTESIAN_POINT('Ctrl Pts',(62.3780831265606,2.97770365011463,338.91679638585));
#31390=CARTESIAN_POINT('Ctrl Pts',(62.3703342415325,3.0858365479526,338.832179007672));
#31391=CARTESIAN_POINT('Ctrl Pts',(62.3625853565044,3.19019247576707,338.743241246575));
#31392=CARTESIAN_POINT('Ctrl Pts',(62.3548282467297,3.29465916804167,338.654209086019));
#31393=CARTESIAN_POINT('Ctrl Pts',(62.347071136955,3.39534058414771,338.56084763612));
#31394=CARTESIAN_POINT('Ctrl Pts',(62.3393140271802,3.49187382520074,338.463524253037));
#31395=CARTESIAN_POINT('Ctrl Pts',(62.3315527722541,3.58845865053107,338.366148863451));
#31396=CARTESIAN_POINT('Ctrl Pts',(62.3237915173279,3.68089062065925,338.264807610753));
#31397=CARTESIAN_POINT('Ctrl Pts',(62.3160302624018,3.76884640471999,338.159901871915));
#31398=CARTESIAN_POINT('Ctrl Pts',(62.3082565919971,3.85694288937075,338.054828318082));
#31399=CARTESIAN_POINT('Ctrl Pts',(62.3004829215924,3.94054864077809,337.946179193729));
#31400=CARTESIAN_POINT('Ctrl Pts',(62.2927092511878,4.01938251549385,337.834386575018));
#31401=CARTESIAN_POINT('Ctrl Pts',(62.2852974470106,4.09454665437628,337.727797929602));
#31402=CARTESIAN_POINT('Ctrl Pts',(62.2778856428334,4.16537302409506,337.618352104653));
#31403=CARTESIAN_POINT('Ctrl Pts',(62.2704738386562,4.23165728892461,337.506443626254));
#31404=CARTESIAN_POINT('Ctrl Pts',(62.2626987598778,4.30119034302321,337.389050179972));
#31405=CARTESIAN_POINT('Ctrl Pts',(62.2549236810993,4.36594452734166,337.268575587395));
#31406=CARTESIAN_POINT('Ctrl Pts',(62.2471486023209,4.42563478496584,337.145446296834));
#31407=CARTESIAN_POINT('Ctrl Pts',(62.2393830912719,4.48525158992794,337.022468524705));
#31408=CARTESIAN_POINT('Ctrl Pts',(62.2316175802228,4.53981669818476,336.896842902899));
#31409=CARTESIAN_POINT('Ctrl Pts',(62.2238520691738,4.58908914001719,336.769023438928));
#31410=CARTESIAN_POINT('Ctrl Pts',(62.2160942576517,4.63831272807992,336.641330708328));
#31411=CARTESIAN_POINT('Ctrl Pts',(62.2083364461295,4.68225395324022,336.511448826702));
#31412=CARTESIAN_POINT('Ctrl Pts',(62.2005786346073,4.72071863037156,336.379854584861));
#31413=CARTESIAN_POINT('Ctrl Pts',(62.1928266610843,4.7591543616135,336.248359371861));
#31414=CARTESIAN_POINT('Ctrl Pts',(62.1850746875613,4.79212163880366,336.115154737217));
#31415=CARTESIAN_POINT('Ctrl Pts',(62.1773227140384,4.81947523052142,335.980735216504));
#31416=CARTESIAN_POINT('Ctrl Pts',(62.1695740234807,4.84681723797698,335.846372622536));
#31417=CARTESIAN_POINT('Ctrl Pts',(62.1618253329231,4.86855021065845,335.71079654804));
#31418=CARTESIAN_POINT('Ctrl Pts',(62.1540766423655,4.88457946323702,335.574514168514));
#31419=CARTESIAN_POINT('Ctrl Pts',(62.1463295639876,4.9006053807957,335.438260143676));
#31420=CARTESIAN_POINT('Ctrl Pts',(62.1385824856098,4.91092989306442,335.301300494062));
#31421=CARTESIAN_POINT('Ctrl Pts',(62.1308354072319,4.91550993953144,335.164149617324));
#31422=CARTESIAN_POINT('Ctrl Pts',(62.1230882639261,4.92009002438368,335.026997591129));
#31423=CARTESIAN_POINT('Ctrl Pts',(62.1153411206204,4.9189255343614,334.88965472527));
#31424=CARTESIAN_POINT('Ctrl Pts',(62.1075939773145,4.91202551667773,334.752637136969));
#31425=CARTESIAN_POINT('Ctrl Pts',(62.0998450922865,4.90512394772362,334.615588744206));
#31426=CARTESIAN_POINT('Ctrl Pts',(62.0920962072584,4.89248430486528,334.478866164824));
#31427=CARTESIAN_POINT('Ctrl Pts',(62.0843473222303,4.8741676246373,334.342981713011));
#31428=CARTESIAN_POINT('Ctrl Pts',(62.0765902124555,4.8558315028956,334.206953032037));
#31429=CARTESIAN_POINT('Ctrl Pts',(62.0688331026808,4.83180635924938,334.07176464367));
#31430=CARTESIAN_POINT('Ctrl Pts',(62.0610759929061,4.80220472592158,333.937920514822));
#31431=CARTESIAN_POINT('Ctrl Pts',(62.0533147379799,4.77258727442745,333.80400486395));
#31432=CARTESIAN_POINT('Ctrl Pts',(62.0455534830537,4.73738749579509,333.671435281525));
#31433=CARTESIAN_POINT('Ctrl Pts',(62.0377922281276,4.69676794359653,333.540700871478));
#31434=CARTESIAN_POINT('Ctrl Pts',(62.0300185577229,4.65608341335234,333.409757328981));
#31435=CARTESIAN_POINT('Ctrl Pts',(62.0222448873183,4.60996191614014,333.2806551935));
#31436=CARTESIAN_POINT('Ctrl Pts',(62.0144712169136,4.55861465117034,333.153864705761));
#31437=CARTESIAN_POINT('Ctrl Pts',(62.0070594127365,4.50965761373842,333.03297634573));
#31438=CARTESIAN_POINT('Ctrl Pts',(61.9996476085594,4.45595049728665,332.914189524542));
#31439=CARTESIAN_POINT('Ctrl Pts',(61.9922358043824,4.39771448942881,332.797889573167));
#31440=CARTESIAN_POINT('Ctrl Pts',(61.9844607256039,4.33662416134957,332.675889414735));
#31441=CARTESIAN_POINT('Ctrl Pts',(61.9766856468255,4.27035671096763,332.556240524797));
#31442=CARTESIAN_POINT('Ctrl Pts',(61.9689105680471,4.19911648711376,332.439413389446));
#31443=CARTESIAN_POINT('Ctrl Pts',(61.9611450569981,4.12796392889081,332.322730017322));
#31444=CARTESIAN_POINT('Ctrl Pts',(61.9533795459491,4.05185097443223,332.208861821338));
#31445=CARTESIAN_POINT('Ctrl Pts',(61.9456140349,3.97102900579846,332.098257127586));
#31446=CARTESIAN_POINT('Ctrl Pts',(61.9378562233779,3.89028717238233,331.98776209871));
#31447=CARTESIAN_POINT('Ctrl Pts',(61.9300984118557,3.8048458454959,331.880524446259));
#31448=CARTESIAN_POINT('Ctrl Pts',(61.9223406003336,3.71500088399098,331.776965483516));
#31449=CARTESIAN_POINT('Ctrl Pts',(61.9145886268106,3.62522353366838,331.673484452176));
#31450=CARTESIAN_POINT('Ctrl Pts',(61.9068366532876,3.53104939994974,331.573676894374));
#31451=CARTESIAN_POINT('Ctrl Pts',(61.8990846797646,3.43281575529389,331.477932559887));
#31452=CARTESIAN_POINT('Ctrl Pts',(61.891335989207,3.3346237126448,331.382228773181));
#31453=CARTESIAN_POINT('Ctrl Pts',(61.8835872986494,3.23237585776785,331.290585059537));
#31454=CARTESIAN_POINT('Ctrl Pts',(61.8758386080918,3.12644744569646,331.203355503632));
#31455=CARTESIAN_POINT('Ctrl Pts',(61.8680915297139,3.02054107291607,331.116144096565));
#31456=CARTESIAN_POINT('Ctrl Pts',(61.8603444513361,2.91095596765934,331.033345268786));
#31457=CARTESIAN_POINT('Ctrl Pts',(61.8525973729583,2.79810139537135,330.955273600882));
#31458=CARTESIAN_POINT('Ctrl Pts',(61.8448502296525,2.68524587725349,330.877201278663));
#31459=CARTESIAN_POINT('Ctrl Pts',(61.8371030863468,2.56912115890212,330.803856417718));
#31460=CARTESIAN_POINT('Ctrl Pts',(61.829355943041,2.45016615026692,330.735510710696));
#31461=CARTESIAN_POINT('Ctrl Pts',(61.8216070580129,2.33118439802006,330.667149638109));
#31462=CARTESIAN_POINT('Ctrl Pts',(61.8138581729848,2.20937142815575,330.603790150599));
#31463=CARTESIAN_POINT('Ctrl Pts',(61.8061092879567,2.08519108697685,330.545658163848));
#31464=CARTESIAN_POINT('Ctrl Pts',(61.798352178182,1.96087893950071,330.487464475206));
#31465=CARTESIAN_POINT('Ctrl Pts',(61.7905950684072,1.83419475581605,330.434509536998));
#31466=CARTESIAN_POINT('Ctrl Pts',(61.7828379586325,1.70562323009318,330.386971443892));
#31467=CARTESIAN_POINT('Ctrl Pts',(61.7750767037064,1.57698299985807,330.339407947949));
#31468=CARTESIAN_POINT('Ctrl Pts',(61.7673154487802,1.44645378976839,330.297267184864));
#31469=CARTESIAN_POINT('Ctrl Pts',(61.7595541938541,1.31453486481976,330.260677142073));
#31470=CARTESIAN_POINT('Ctrl Pts',(61.7517805234494,1.18240491258339,330.224028567137));
#31471=CARTESIAN_POINT('Ctrl Pts',(61.7440068530448,1.04888118399147,330.192948544714));
#31472=CARTESIAN_POINT('Ctrl Pts',(61.7362331826401,0.914473406514856,330.16751394712));
#31473=CARTESIAN_POINT('Ctrl Pts',(61.7288213784629,0.786322343413962,330.143263336163));
#31474=CARTESIAN_POINT('Ctrl Pts',(61.7214095742857,0.657367968842301,330.124144431247));
#31475=CARTESIAN_POINT('Ctrl Pts',(61.7139977701084,0.528054013144585,330.110179755686));
#31476=CARTESIAN_POINT('Ctrl Pts',(61.70622269133,0.392401995274051,330.095530629778));
#31477=CARTESIAN_POINT('Ctrl Pts',(61.6984476125515,0.255925571301257,330.086507462761));
#31478=CARTESIAN_POINT('Ctrl Pts',(61.6906725337731,0.119130967896039,330.083193020365));
#31479=CARTESIAN_POINT('Ctrl Pts',(61.6829070227241,-0.0174953010410114,
330.079882656601));
#31480=CARTESIAN_POINT('Ctrl Pts',(61.6751415116751,-0.154438583333955,
330.082267049201));
#31481=CARTESIAN_POINT('Ctrl Pts',(61.667376000626,-0.291185834749258,330.090377420601));
#31482=CARTESIAN_POINT('Ctrl Pts',(61.6596181891038,-0.427797500866653,
330.098479750545));
#31483=CARTESIAN_POINT('Ctrl Pts',(61.6518603775816,-0.56421313522898,330.112296738098));
#31484=CARTESIAN_POINT('Ctrl Pts',(61.6441025660594,-0.699918340307498,
330.131807586033));
#31485=CARTESIAN_POINT('Ctrl Pts',(61.6363505925364,-0.83552142291629,330.151303751437));
#31486=CARTESIAN_POINT('Ctrl Pts',(61.6285986190133,-0.970414755039212,
330.176485193116));
#31487=CARTESIAN_POINT('Ctrl Pts',(61.6208466454903,-1.1040880702953,330.20727920743));
#31488=CARTESIAN_POINT('Ctrl Pts',(61.6130979549326,-1.23770477482239,330.238060180461));
#31489=CARTESIAN_POINT('Ctrl Pts',(61.605349264375,-1.37010211001328,330.274448911022));
#31490=CARTESIAN_POINT('Ctrl Pts',(61.5976005738174,-1.50077924647777,330.316321454685));
#31491=CARTESIAN_POINT('Ctrl Pts',(61.5898534954396,-1.6314291944724,330.358185286416));
#31492=CARTESIAN_POINT('Ctrl Pts',(61.5821064170618,-1.76035928363424,330.405530542616));
#31493=CARTESIAN_POINT('Ctrl Pts',(61.5743593386839,-1.88708349941958,330.458183300846));
#31494=CARTESIAN_POINT('Ctrl Pts',(61.5666121953782,-2.01380877727573,330.510836500356));
#31495=CARTESIAN_POINT('Ctrl Pts',(61.5588650520723,-2.13832778392347,330.568797140646));
#31496=CARTESIAN_POINT('Ctrl Pts',(61.5511179087665,-2.26017452785904,330.631843161456));
#31497=CARTESIAN_POINT('Ctrl Pts',(61.5433690237384,-2.3820486655297,330.694903356351));
#31498=CARTESIAN_POINT('Ctrl Pts',(61.5356201387103,-2.50124899791215,330.763051027218));
#31499=CARTESIAN_POINT('Ctrl Pts',(61.5278712536822,-2.61733453384105,330.836018371743));
#31500=CARTESIAN_POINT('Ctrl Pts',(61.5201141439075,-2.73354328415734,330.909063164562));
#31501=CARTESIAN_POINT('Ctrl Pts',(61.5123570341327,-2.84663030236878,330.986937641693));
#31502=CARTESIAN_POINT('Ctrl Pts',(61.504599924358,-2.95618352904371,331.069330590712));
#31503=CARTESIAN_POINT('Ctrl Pts',(61.4968386694318,-3.06579529745992,331.151767567889));
#31504=CARTESIAN_POINT('Ctrl Pts',(61.4890774145057,-3.17186920951577,331.23872758043));
#31505=CARTESIAN_POINT('Ctrl Pts',(61.4813161595796,-3.27402745690945,331.329860047096));
#31506=CARTESIAN_POINT('Ctrl Pts',(61.4735424891749,-3.37634912420559,331.421138296008));
#31507=CARTESIAN_POINT('Ctrl Pts',(61.4657688187702,-3.47474232925547,331.516602064481));
#31508=CARTESIAN_POINT('Ctrl Pts',(61.4579951483656,-3.56886658570419,331.61586431183));
#31509=CARTESIAN_POINT('Ctrl Pts',(61.4505833441886,-3.65860933536932,331.710505877684));
#31510=CARTESIAN_POINT('Ctrl Pts',(61.4431715400116,-3.74447144187631,331.808600025886));
#31511=CARTESIAN_POINT('Ctrl Pts',(61.4357597358346,-3.82619383693742,331.909785802783));
#31512=CARTESIAN_POINT('Ctrl Pts',(61.4278754238619,-3.91312609289425,332.017422245031));
#31513=CARTESIAN_POINT('Ctrl Pts',(61.4199911118892,-3.99566014173165,332.1289122848));
#31514=CARTESIAN_POINT('Ctrl Pts',(61.4121067999165,-4.07343455458442,332.243858858473));
#31515=CARTESIAN_POINT('Ctrl Pts',(61.4043645082339,-4.14980801517776,332.356734896912));
#31516=CARTESIAN_POINT('Ctrl Pts',(61.3966222165512,-4.22159159652285,332.472943674719));
#31517=CARTESIAN_POINT('Ctrl Pts',(61.3888799248686,-4.28848152717237,332.592073661093));
#31518=CARTESIAN_POINT('Ctrl Pts',(61.381145075822,-4.35530715678206,332.711089128258));
#31519=CARTESIAN_POINT('Ctrl Pts',(61.3734102267753,-4.41724830220632,332.833019877969));
#31520=CARTESIAN_POINT('Ctrl Pts',(61.3656753777287,-4.47404401241101,332.957424851441));
#31521=CARTESIAN_POINT('Ctrl Pts',(61.3579462672387,-4.53079758534822,333.081737527703));
#31522=CARTESIAN_POINT('Ctrl Pts',(61.3502171567488,-4.58241315598515,333.208520419483));
#31523=CARTESIAN_POINT('Ctrl Pts',(61.3424880462589,-4.62867553359679,333.337307645058));
#31524=CARTESIAN_POINT('Ctrl Pts',(61.3344920631115,-4.67653527013741,333.470541668124));
#31525=CARTESIAN_POINT('Ctrl Pts',(61.326496079964,-4.71866527595313,333.605920551521));
#31526=CARTESIAN_POINT('Ctrl Pts',(61.3185000968166,-4.75488129027722,333.742905342517));
#31527=CARTESIAN_POINT('Ctrl Pts',(61.3107765708199,-4.78986327097582,333.875222479123));
#31528=CARTESIAN_POINT('Ctrl Pts',(61.3030530448233,-4.81932759969248,334.009037463177));
#31529=CARTESIAN_POINT('Ctrl Pts',(61.2953295188266,-4.84315901522016,334.143849419908));
#31530=CARTESIAN_POINT('Ctrl Pts',(61.2876066690408,-4.86698834425729,334.278649573568));
#31531=CARTESIAN_POINT('Ctrl Pts',(61.2798838192551,-4.88518567836036,334.41444613842));
#31532=CARTESIAN_POINT('Ctrl Pts',(61.2721609694693,-4.89768709330298,334.550729259139));
#31533=CARTESIAN_POINT('Ctrl Pts',(61.264435857073,-4.91019217086169,334.687052307559));
#31534=CARTESIAN_POINT('Ctrl Pts',(61.2567107446767,-4.91699796774325,334.823861804713));
#31535=CARTESIAN_POINT('Ctrl Pts',(61.2489856322803,-4.91809253490547,334.960644179502));
#31536=CARTESIAN_POINT('Ctrl Pts',(61.2481691710169,-4.91820821887774,334.975100604834));
#31537=CARTESIAN_POINT('Ctrl Pts',(61.2473527097534,-4.91826015516819,334.989556727422));
#31538=CARTESIAN_POINT('Ctrl Pts',(61.24653624849,-4.9182483636783,335.00401194164));
#31539=CARTESIAN_POINT('',(64.7465362484525,-4.91824918766967,334.997173255123));
#31540=CARTESIAN_POINT('Ctrl Pts',(64.7465362484525,-4.91824918766967,334.997173255123));
#31541=CARTESIAN_POINT('Ctrl Pts',(64.7388635417342,-4.91832669084382,335.132020911997));
#31542=CARTESIAN_POINT('Ctrl Pts',(64.731190835016,-4.91285417304389,335.267091728814));
#31543=CARTESIAN_POINT('Ctrl Pts',(64.7235181282978,-4.9018029748704,335.40188388628));
#31544=CARTESIAN_POINT('Ctrl Pts',(64.715853995146,-4.89076412542671,335.536525425515));
#31545=CARTESIAN_POINT('Ctrl Pts',(64.7081898619942,-4.87415902608872,335.670888527897));
#31546=CARTESIAN_POINT('Ctrl Pts',(64.7005257288424,-4.85201102103137,335.804470082906));
#31547=CARTESIAN_POINT('Ctrl Pts',(64.6928682158542,-4.82988214708956,335.937936252164));
#31548=CARTESIAN_POINT('Ctrl Pts',(64.685210702866,-4.80221995721399,336.070621822914));
#31549=CARTESIAN_POINT('Ctrl Pts',(64.6775531898779,-4.76909967332192,336.202028023143));
#31550=CARTESIAN_POINT('Ctrl Pts',(64.6698999197036,-4.73599774045353,336.333361414869));
#31551=CARTESIAN_POINT('Ctrl Pts',(64.6622466495294,-4.69744382577316,336.463416457486));
#31552=CARTESIAN_POINT('Ctrl Pts',(64.6545933793552,-4.65356430540468,336.591704218115));
#31553=CARTESIAN_POINT('Ctrl Pts',(64.6469422691734,-4.60969716921042,336.719955771921));
#31554=CARTESIAN_POINT('Ctrl Pts',(64.6392911589915,-4.56050754533228,336.846440655695));
#31555=CARTESIAN_POINT('Ctrl Pts',(64.6316400488097,-4.50617163613448,336.970685223012));
#31556=CARTESIAN_POINT('Ctrl Pts',(64.6239893429186,-4.45183859808905,337.094923225148));
#31557=CARTESIAN_POINT('Ctrl Pts',(64.6163386370275,-4.39235997645717,337.216920778271));
#31558=CARTESIAN_POINT('Ctrl Pts',(64.6086879311364,-4.32795985513916,337.33622485108));
#31559=CARTESIAN_POINT('Ctrl Pts',(64.6010358743879,-4.26354836292587,337.455549988975));
#31560=CARTESIAN_POINT('Ctrl Pts',(64.5933838176395,-4.19421383407427,337.572180347593));
#31561=CARTESIAN_POINT('Ctrl Pts',(64.585731760891,-4.12022570570791,337.685688588896));
#31562=CARTESIAN_POINT('Ctrl Pts',(64.5780719696904,-4.04616279252726,337.799311560668));
#31563=CARTESIAN_POINT('Ctrl Pts',(64.5704121784898,-3.96743710541301,337.909805775638));
#31564=CARTESIAN_POINT('Ctrl Pts',(64.5627523872891,-3.88436093284001,338.016773641811));
#31565=CARTESIAN_POINT('Ctrl Pts',(64.5550886535452,-3.80124200043196,338.123796565026));
#31566=CARTESIAN_POINT('Ctrl Pts',(64.5474249198012,-3.71376838271351,338.227289218797));
#31567=CARTESIAN_POINT('Ctrl Pts',(64.5397611860573,-3.62229101222018,338.326889070181));
#31568=CARTESIAN_POINT('Ctrl Pts',(64.5320854558956,-3.53067044771968,338.426644830089));
#31569=CARTESIAN_POINT('Ctrl Pts',(64.524409725734,-3.43503389460652,338.522495331051));
#31570=CARTESIAN_POINT('Ctrl Pts',(64.5167339955724,-3.33576779431985,338.614116252264));
#31571=CARTESIAN_POINT('Ctrl Pts',(64.5099487013309,-3.24801722408502,338.695108535215));
#31572=CARTESIAN_POINT('Ctrl Pts',(64.5031634070894,-3.15743100405289,338.77279611708));
#31573=CARTESIAN_POINT('Ctrl Pts',(64.4963781128479,-3.06429501471525,338.846983119964));
#31574=CARTESIAN_POINT('Ctrl Pts',(64.4886030340694,-2.9575730910322,338.931991930376));
#31575=CARTESIAN_POINT('Ctrl Pts',(64.480827955291,-2.84714241004196,339.012690731727));
#31576=CARTESIAN_POINT('Ctrl Pts',(64.4730528765125,-2.7333861914832,339.088738557393));
#31577=CARTESIAN_POINT('Ctrl Pts',(64.4652873654635,-2.61976995719346,339.164692801367));
#31578=CARTESIAN_POINT('Ctrl Pts',(64.4575218544145,-2.50283664965343,339.236007242268));
#31579=CARTESIAN_POINT('Ctrl Pts',(64.4497563433655,-2.38300284600843,339.302380794213));
#31580=CARTESIAN_POINT('Ctrl Pts',(64.4419985318433,-2.26328785792879,339.368688536589));
#31581=CARTESIAN_POINT('Ctrl Pts',(64.4342407203211,-2.14067843657487,339.430064950941));
#31582=CARTESIAN_POINT('Ctrl Pts',(64.4264829087989,-2.01562015668641,339.486252160374));
#31583=CARTESIAN_POINT('Ctrl Pts',(64.4187309352759,-1.89065598711913,339.54239708715));
#31584=CARTESIAN_POINT('Ctrl Pts',(64.4109789617528,-1.76324698221357,339.593360422256));
#31585=CARTESIAN_POINT('Ctrl Pts',(64.4032269882298,-1.63386302173005,339.638930338852));
#31586=CARTESIAN_POINT('Ctrl Pts',(64.3954782976722,-1.50453385543096,339.684480956562));
#31587=CARTESIAN_POINT('Ctrl Pts',(64.3877296071146,-1.37323176499267,339.724642569129));
#31588=CARTESIAN_POINT('Ctrl Pts',(64.379980916557,-1.24044609768678,339.759251678703));
#31589=CARTESIAN_POINT('Ctrl Pts',(64.3722338381791,-1.10768805754793,339.793853587562));
#31590=CARTESIAN_POINT('Ctrl Pts',(64.3644867598013,-0.973447432509595,
339.822905192771));
#31591=CARTESIAN_POINT('Ctrl Pts',(64.3567396814234,-0.838227819271319,
339.846293138627));
#31592=CARTESIAN_POINT('Ctrl Pts',(64.3489925381176,-0.703007072762353,
339.869681280496));
#31593=CARTESIAN_POINT('Ctrl Pts',(64.3412453948118,-0.566807706843793,
339.887405601719));
#31594=CARTESIAN_POINT('Ctrl Pts',(64.333498251506,-0.430142183666102,339.899404123394));
#31595=CARTESIAN_POINT('Ctrl Pts',(64.3257493664779,-0.293445935177217,
339.911405342592));
#31596=CARTESIAN_POINT('Ctrl Pts',(64.3180004814498,-0.156283710185274,
339.917678166518));
#31597=CARTESIAN_POINT('Ctrl Pts',(64.3102515964217,-0.0191713498283948,
339.918212634875));
#31598=CARTESIAN_POINT('Ctrl Pts',(64.3024944866469,0.118086543004216,339.918747670522));
#31599=CARTESIAN_POINT('Ctrl Pts',(64.2947373768722,0.255294073986738,339.91353218223));
#31600=CARTESIAN_POINT('Ctrl Pts',(64.2869802670974,0.391936591957358,339.902608363961));
#31601=CARTESIAN_POINT('Ctrl Pts',(64.2792190121713,0.528652127320508,339.891678708354));
#31602=CARTESIAN_POINT('Ctrl Pts',(64.2714577572451,0.664801660270137,339.875034692081));
#31603=CARTESIAN_POINT('Ctrl Pts',(64.263696502319,0.799878386127947,339.852770098604));
#31604=CARTESIAN_POINT('Ctrl Pts',(64.2559228319143,0.935171190725635,339.830469889034));
#31605=CARTESIAN_POINT('Ctrl Pts',(64.2481491615096,1.06938737599947,339.802531215094));
#31606=CARTESIAN_POINT('Ctrl Pts',(64.240375491105,1.20203213510304,339.769098636921));
#31607=CARTESIAN_POINT('Ctrl Pts',(64.232963686928,1.32850224875641,339.737222353305));
#31608=CARTESIAN_POINT('Ctrl Pts',(64.225551882751,1.45354366758471,339.700352218741));
#31609=CARTESIAN_POINT('Ctrl Pts',(64.218140078574,1.5767443156899,339.658654357799));
#31610=CARTESIAN_POINT('Ctrl Pts',(64.2103649997955,1.70598339455634,339.61491276048));
#31611=CARTESIAN_POINT('Ctrl Pts',(64.2025899210171,1.83360511624078,339.565719996807));
#31612=CARTESIAN_POINT('Ctrl Pts',(64.1948148422386,1.95911537244465,339.511213807829));
#31613=CARTESIAN_POINT('Ctrl Pts',(64.1870493311896,2.08447118028754,339.456774692187));
#31614=CARTESIAN_POINT('Ctrl Pts',(64.1792838201406,2.20772033740928,339.397035315208));
#31615=CARTESIAN_POINT('Ctrl Pts',(64.1715183090916,2.32838422047214,339.332183050652));
#31616=CARTESIAN_POINT('Ctrl Pts',(64.1637604975694,2.44892846494381,339.267395087305));
#31617=CARTESIAN_POINT('Ctrl Pts',(64.1560026860472,2.56689219440278,339.197504508715));
#31618=CARTESIAN_POINT('Ctrl Pts',(64.148244874525,2.68181742860675,339.122746456201));
#31619=CARTESIAN_POINT('Ctrl Pts',(64.140492901002,2.79665617792788,339.048044661492));
#31620=CARTESIAN_POINT('Ctrl Pts',(64.132740927479,2.90846065695497,338.968482896016));
#31621=CARTESIAN_POINT('Ctrl Pts',(64.1249889539559,3.01679845708052,338.884341660032));
#31622=CARTESIAN_POINT('Ctrl Pts',(64.1172402633983,3.12509037608303,338.80023605791));
#31623=CARTESIAN_POINT('Ctrl Pts',(64.1094915728406,3.22991822814946,338.711555081886));
#31624=CARTESIAN_POINT('Ctrl Pts',(64.101742882283,3.33087971056249,338.618621756451));
#31625=CARTESIAN_POINT('Ctrl Pts',(64.0939958039052,3.431820187096,338.525707766571));
#31626=CARTESIAN_POINT('Ctrl Pts',(64.0862487255273,3.52889560663854,338.428543451637));
#31627=CARTESIAN_POINT('Ctrl Pts',(64.0785016471495,3.62173812089176,338.327490953583));
#31628=CARTESIAN_POINT('Ctrl Pts',(64.0707545038437,3.71458141325461,338.226437608613));
#31629=CARTESIAN_POINT('Ctrl Pts',(64.0630073605378,3.80319146511906,338.121496303361));
#31630=CARTESIAN_POINT('Ctrl Pts',(64.055260217232,3.88723883443075,338.013064437843));
#31631=CARTESIAN_POINT('Ctrl Pts',(64.0475113322039,3.9713050993756,337.90460819454));
#31632=CARTESIAN_POINT('Ctrl Pts',(64.0397624471758,4.05080640115004,337.792660138277));
#31633=CARTESIAN_POINT('Ctrl Pts',(64.0320135621476,4.12545521268858,337.677648660784));
#31634=CARTESIAN_POINT('Ctrl Pts',(64.0242564523729,4.20018325724675,337.562515108922));
#31635=CARTESIAN_POINT('Ctrl Pts',(64.0164993425982,4.27004830985525,337.444311968944));
#31636=CARTESIAN_POINT('Ctrl Pts',(64.0087422328234,4.33480734504369,337.323494855569));
#31637=CARTESIAN_POINT('Ctrl Pts',(64.0009809778973,4.39960098538997,337.202613181391));
#31638=CARTESIAN_POINT('Ctrl Pts',(63.9932197229711,4.45928300155939,337.079115102272));
#31639=CARTESIAN_POINT('Ctrl Pts',(63.9854584680449,4.51365799697293,336.95347755269));
#31640=CARTESIAN_POINT('Ctrl Pts',(63.9776847976402,4.56811997465828,336.827639023974));
#31641=CARTESIAN_POINT('Ctrl Pts',(63.9699111272355,4.61725782687195,336.69965455081));
#31642=CARTESIAN_POINT('Ctrl Pts',(63.9621374568309,4.66092534893875,336.570018456618));
#31643=CARTESIAN_POINT('Ctrl Pts',(63.9547256526539,4.70256013734701,336.4464169538));
#31644=CARTESIAN_POINT('Ctrl Pts',(63.9473138484769,4.73922234120536,336.321314411645));
#31645=CARTESIAN_POINT('Ctrl Pts',(63.9399020442999,4.77082866029556,336.195147253104));
#31646=CARTESIAN_POINT('Ctrl Pts',(63.9321269655215,4.80398409923516,336.062796266289));
#31647=CARTESIAN_POINT('Ctrl Pts',(63.924351886743,4.83168029131735,335.928855410731));
#31648=CARTESIAN_POINT('Ctrl Pts',(63.9165768079646,4.85376567557622,335.793814732225));
#31649=CARTESIAN_POINT('Ctrl Pts',(63.9088112969156,4.87582388236372,335.658940229872));
#31650=CARTESIAN_POINT('Ctrl Pts',(63.9010457858666,4.89228495673134,335.522968979514));
#31651=CARTESIAN_POINT('Ctrl Pts',(63.8932802748176,4.90304745472148,335.386404864422));
#31652=CARTESIAN_POINT('Ctrl Pts',(63.8855224632954,4.91379928166351,335.249976153048));
#31653=CARTESIAN_POINT('Ctrl Pts',(63.8777646517732,4.91886374584472,335.112956133905));
#31654=CARTESIAN_POINT('Ctrl Pts',(63.8700068402511,4.91819074322881,334.97585718081));
#31655=CARTESIAN_POINT('Ctrl Pts',(63.862254866728,4.91751824706871,334.838861399024));
#31656=CARTESIAN_POINT('Ctrl Pts',(63.854502893205,4.91111688004535,334.701787190814));
#31657=CARTESIAN_POINT('Ctrl Pts',(63.846750919682,4.89898851970082,334.565149972589));
#31658=CARTESIAN_POINT('Ctrl Pts',(63.8390022291243,4.88686529572412,334.428570620307));
#31659=CARTESIAN_POINT('Ctrl Pts',(63.8312535385667,4.86901993683374,334.29242827846));
#31660=CARTESIAN_POINT('Ctrl Pts',(63.8235048480091,4.84550637213241,334.157236059075));
#31661=CARTESIAN_POINT('Ctrl Pts',(63.8157577696313,4.8219976996246,334.022071967559));
#31662=CARTESIAN_POINT('Ctrl Pts',(63.8080106912535,4.79282323398786,333.887857990155));
#31663=CARTESIAN_POINT('Ctrl Pts',(63.8002636128756,4.75808844427899,333.755099434124));
#31664=CARTESIAN_POINT('Ctrl Pts',(63.7925164695698,4.72335336345914,333.622339765448));
#31665=CARTESIAN_POINT('Ctrl Pts',(63.784769326264,4.6830579645558,333.49103592062));
#31666=CARTESIAN_POINT('Ctrl Pts',(63.7770221829582,4.6373581497214,333.361679990444));
#31667=CARTESIAN_POINT('Ctrl Pts',(63.7692732979302,4.59164806059842,333.232294978308));
#31668=CARTESIAN_POINT('Ctrl Pts',(63.7615244129021,4.54053126795435,333.104859120739));
#31669=CARTESIAN_POINT('Ctrl Pts',(63.753775527874,4.48421241814045,332.979846032726));
#31670=CARTESIAN_POINT('Ctrl Pts',(63.7460184180992,4.42783379091744,332.854700254529));
#31671=CARTESIAN_POINT('Ctrl Pts',(63.7382613083245,4.36624223757976,332.731982739749));
#31672=CARTESIAN_POINT('Ctrl Pts',(63.7305041985498,4.29968937923557,332.612144412954));
#31673=CARTESIAN_POINT('Ctrl Pts',(63.7227429436236,4.23310095717178,332.492242048388));
#31674=CARTESIAN_POINT('Ctrl Pts',(63.7149816886975,4.16154615122746,332.375222270802));
#31675=CARTESIAN_POINT('Ctrl Pts',(63.7072204337713,4.08532028547939,332.261507489959));
#31676=CARTESIAN_POINT('Ctrl Pts',(63.6994467633666,4.00897248318813,332.147610802527));
#31677=CARTESIAN_POINT('Ctrl Pts',(63.691673092962,3.92793892063876,332.037029992114));
#31678=CARTESIAN_POINT('Ctrl Pts',(63.6838994225573,3.84255616519977,331.930155512117));
#31679=CARTESIAN_POINT('Ctrl Pts',(63.6764876183802,3.76114799756813,331.828256064876));
#31680=CARTESIAN_POINT('Ctrl Pts',(63.6690758142031,3.67578662310787,331.729725871554));
#31681=CARTESIAN_POINT('Ctrl Pts',(63.661664010026,3.58679396066131,331.634871154582));
#31682=CARTESIAN_POINT('Ctrl Pts',(63.6538889312476,3.49343950273298,331.535367325374));
#31683=CARTESIAN_POINT('Ctrl Pts',(63.6461138524692,3.39579377853452,331.439593924113));
#31684=CARTESIAN_POINT('Ctrl Pts',(63.6383387736907,3.29418685969407,331.347943593546));
#31685=CARTESIAN_POINT('Ctrl Pts',(63.6305732626417,3.19270497463588,331.256406044547));
#31686=CARTESIAN_POINT('Ctrl Pts',(63.6228077515927,3.08727188126725,331.168981730332));
#31687=CARTESIAN_POINT('Ctrl Pts',(63.6150422405437,2.9782564086333,331.086028637441));
#31688=CARTESIAN_POINT('Ctrl Pts',(63.6072844290216,2.86934902515838,331.003157792783));
#31689=CARTESIAN_POINT('Ctrl Pts',(63.5995266174994,2.75686664003477,330.924749582242));
#31690=CARTESIAN_POINT('Ctrl Pts',(63.5917688059772,2.64121300516677,330.851123414244));
#31691=CARTESIAN_POINT('Ctrl Pts',(63.5840168324542,2.52564640332603,330.777552652271));
#31692=CARTESIAN_POINT('Ctrl Pts',(63.5762648589312,2.40691363028603,330.708756978989));
#31693=CARTESIAN_POINT('Ctrl Pts',(63.5685128854082,2.28544912674577,330.645013736927));
#31694=CARTESIAN_POINT('Ctrl Pts',(63.5607641948506,2.16403606349503,330.581297490165));
#31695=CARTESIAN_POINT('Ctrl Pts',(63.553015504293,2.03989391610473,330.522629600151));
#31696=CARTESIAN_POINT('Ctrl Pts',(63.5452668137354,1.91348335555601,330.469242391111));
#31697=CARTESIAN_POINT('Ctrl Pts',(63.5375197353576,1.7870990957803,330.415866289725));
#31698=CARTESIAN_POINT('Ctrl Pts',(63.5297726569797,1.65844772146513,330.367768835919));
#31699=CARTESIAN_POINT('Ctrl Pts',(63.5220255786019,1.52801123162574,330.325134789267));
#31700=CARTESIAN_POINT('Ctrl Pts',(63.5142784352961,1.39757364860275,330.2825003853));
#31701=CARTESIAN_POINT('Ctrl Pts',(63.5065312919903,1.26535129174619,330.245329601253));
#31702=CARTESIAN_POINT('Ctrl Pts',(63.4987841486845,1.13184233831114,330.213757634249));
#31703=CARTESIAN_POINT('Ctrl Pts',(63.4910352636564,0.99830336922879,330.182178569198));
#31704=CARTESIAN_POINT('Ctrl Pts',(63.4832863786283,0.863477608293114,330.156200915862));
#31705=CARTESIAN_POINT('Ctrl Pts',(63.4755374936002,0.727874074336119,330.135908883007));
#31706=CARTESIAN_POINT('Ctrl Pts',(63.4677803838255,0.59212660938732,330.115595311979));
#31707=CARTESIAN_POINT('Ctrl Pts',(63.4600232740507,0.455600109511585,330.100979474401));
#31708=CARTESIAN_POINT('Ctrl Pts',(63.452266164276,0.318809933418614,330.092093797875));
#31709=CARTESIAN_POINT('Ctrl Pts',(63.4445049093499,0.18194666102924,330.083203373128));
#31710=CARTESIAN_POINT('Ctrl Pts',(63.4367436544237,0.0448198222391019,
330.080049219756));
#31711=CARTESIAN_POINT('Ctrl Pts',(63.4289823994975,-0.0920555527655096,
330.082611583604));
#31712=CARTESIAN_POINT('Ctrl Pts',(63.4212087290929,-0.229149883762641,
330.085178046399));
#31713=CARTESIAN_POINT('Ctrl Pts',(63.4134350586882,-0.36599155677716,330.093479276283));
#31714=CARTESIAN_POINT('Ctrl Pts',(63.4056613882835,-0.502070095303246,
330.10744354331));
#31715=CARTESIAN_POINT('Ctrl Pts',(63.3982495841064,-0.631814145122987,
330.120757770347));
#31716=CARTESIAN_POINT('Ctrl Pts',(63.3908377799293,-0.760864224492547,
330.139219629968));
#31717=CARTESIAN_POINT('Ctrl Pts',(63.3834259757521,-0.888788615679096,
330.162724128278));
#31718=CARTESIAN_POINT('Ctrl Pts',(63.3756508969737,-1.02298296234413,330.187380652067));
#31719=CARTESIAN_POINT('Ctrl Pts',(63.3678758181953,-1.1563625629749,330.217664541827));
#31720=CARTESIAN_POINT('Ctrl Pts',(63.3601007394168,-1.28841861521052,330.253510714804));
#31721=CARTESIAN_POINT('Ctrl Pts',(63.3523352283678,-1.42031216406704,330.289312776784));
#31722=CARTESIAN_POINT('Ctrl Pts',(63.3445697173188,-1.55088503157779,330.330663401486));
#31723=CARTESIAN_POINT('Ctrl Pts',(63.3368042062697,-1.67963658466572,330.377446159756));
#31724=CARTESIAN_POINT('Ctrl Pts',(63.3290463947475,-1.80826048021356,330.424182532785));
#31725=CARTESIAN_POINT('Ctrl Pts',(63.3212885832253,-1.9350662900519,330.476340188357));
#31726=CARTESIAN_POINT('Ctrl Pts',(63.3135307717031,-2.05956692349905,330.533752453107));
#31727=CARTESIAN_POINT('Ctrl Pts',(63.3057787981801,-2.18397386627105,330.591121513307));
#31728=CARTESIAN_POINT('Ctrl Pts',(63.2980268246572,-2.3060787320014,330.653737148901));
#31729=CARTESIAN_POINT('Ctrl Pts',(63.2902748511342,-2.42541319665132,330.721384115393));
#31730=CARTESIAN_POINT('Ctrl Pts',(63.2825261605766,-2.54469712308501,330.789002433355));
#31731=CARTESIAN_POINT('Ctrl Pts',(63.2747774700189,-2.66121264265049,330.861647651902));
#31732=CARTESIAN_POINT('Ctrl Pts',(63.2670287794613,-2.77451509344808,330.93905810695));
#31733=CARTESIAN_POINT('Ctrl Pts',(63.2592817010835,-2.88779397072437,331.016452456106));
#31734=CARTESIAN_POINT('Ctrl Pts',(63.2515346227056,-2.99786078640036,331.098609849338));
#31735=CARTESIAN_POINT('Ctrl Pts',(63.2437875443278,-3.10429933488433,331.1852249474));
#31736=CARTESIAN_POINT('Ctrl Pts',(63.236040401022,-3.21073877542587,331.27184077138));
#31737=CARTESIAN_POINT('Ctrl Pts',(63.2282932577162,-3.31354958494718,331.362914127994));
#31738=CARTESIAN_POINT('Ctrl Pts',(63.2205461144104,-3.41234848100445,331.458099252282));
#31739=CARTESIAN_POINT('Ctrl Pts',(63.2127972293822,-3.51116958915165,331.553305776207));
#31740=CARTESIAN_POINT('Ctrl Pts',(63.2050483443541,-3.60597670759358,331.652625636142));
#31741=CARTESIAN_POINT('Ctrl Pts',(63.1972994593259,-3.69642356408649,331.755676357487));
#31742=CARTESIAN_POINT('Ctrl Pts',(63.1895423495512,-3.78696642180693,331.858836457932));
#31743=CARTESIAN_POINT('Ctrl Pts',(63.1817852397765,-3.87313951441264,331.965735035974));
#31744=CARTESIAN_POINT('Ctrl Pts',(63.1740281300017,-3.95463668267359,332.075956263913));
#31745=CARTESIAN_POINT('Ctrl Pts',(63.1662668750755,-4.03617740041542,332.186236390551));
#31746=CARTESIAN_POINT('Ctrl Pts',(63.1585056201494,-4.1130369960825,332.299842381388));
#31747=CARTESIAN_POINT('Ctrl Pts',(63.1507443652232,-4.18495336897915,332.416330446444));
#31748=CARTESIAN_POINT('Ctrl Pts',(63.1429706948185,-4.25698478463489,332.533004854441));
#31749=CARTESIAN_POINT('Ctrl Pts',(63.1351970244139,-4.3240569845687,332.652570208483));
#31750=CARTESIAN_POINT('Ctrl Pts',(63.1274233540092,-4.38595403989221,332.774558420795));
#31751=CARTESIAN_POINT('Ctrl Pts',(63.1200115498322,-4.44496977239846,332.890868052475));
#31752=CARTESIAN_POINT('Ctrl Pts',(63.1125997456551,-4.49928120361495,333.009379788961));
#31753=CARTESIAN_POINT('Ctrl Pts',(63.1051879414781,-4.54874299790963,333.129673771379));
#31754=CARTESIAN_POINT('Ctrl Pts',(63.0961336337335,-4.6091658445539,333.27662567548));
#31755=CARTESIAN_POINT('Ctrl Pts',(63.0870793259888,-4.6625195439318,333.426645313086));
#31756=CARTESIAN_POINT('Ctrl Pts',(63.0780250182441,-4.70851907182097,333.579073818667));
#31757=CARTESIAN_POINT('Ctrl Pts',(63.0693519322519,-4.75258183975855,333.725084488269));
#31758=CARTESIAN_POINT('Ctrl Pts',(63.0606788462596,-4.78989686999387,333.87330508545));
#31759=CARTESIAN_POINT('Ctrl Pts',(63.0520057602673,-4.8202607883652,334.02313307219));
#31760=CARTESIAN_POINT('Ctrl Pts',(63.0433595919639,-4.85053046963215,334.17249605453));
#31761=CARTESIAN_POINT('Ctrl Pts',(63.0347134236606,-4.87389200367215,334.323456262872));
#31762=CARTESIAN_POINT('Ctrl Pts',(63.0260672553572,-4.8901916756631,334.475396875938));
#31763=CARTESIAN_POINT('Ctrl Pts',(63.0174618850766,-4.90641443562036,334.626620538285));
#31764=CARTESIAN_POINT('Ctrl Pts',(63.0088565147959,-4.91564172524436,334.778815161151));
#31765=CARTESIAN_POINT('Ctrl Pts',(63.0002511445153,-4.91777094463565,334.93135600101));
#31766=CARTESIAN_POINT('Ctrl Pts',(62.9990128458577,-4.91807733581093,334.953306377469));
#31767=CARTESIAN_POINT('Ctrl Pts',(62.9977745472,-4.91823683361801,334.975263897979));
#31768=CARTESIAN_POINT('Ctrl Pts',(62.9965362485424,-4.91824921808336,334.997226676644));
#31769=CARTESIAN_POINT('',(66.4965362485266,-4.91824813384112,335.00428444493));
#31770=CARTESIAN_POINT('Ctrl Pts',(66.49653624849,-4.91824813384056,335.004284445576));
#31771=CARTESIAN_POINT('Ctrl Pts',(66.4850389575283,-4.91807160973532,335.20692194809));
#31772=CARTESIAN_POINT('Ctrl Pts',(66.4735416665666,-4.90536856690133,335.409034498468));
#31773=CARTESIAN_POINT('Ctrl Pts',(66.4620443756049,-4.8803514912982,335.609386891788));
#31774=CARTESIAN_POINT('Ctrl Pts',(66.4560443679917,-4.86729601200498,335.713943338107));
#31775=CARTESIAN_POINT('Ctrl Pts',(66.4500443603786,-4.85088762851043,335.818021062282));
#31776=CARTESIAN_POINT('Ctrl Pts',(66.4440443527654,-4.83116108478416,335.921447576028));
#31777=CARTESIAN_POINT('Ctrl Pts',(66.4362692739869,-4.80559854530318,336.055472287993));
#31778=CARTESIAN_POINT('Ctrl Pts',(66.4284941952085,-4.77441427245794,336.188644255654));
#31779=CARTESIAN_POINT('Ctrl Pts',(66.4207191164301,-4.7376767848386,336.320455127939));
#31780=CARTESIAN_POINT('Ctrl Pts',(66.412953605381,-4.70098450503661,336.452103798555));
#31781=CARTESIAN_POINT('Ctrl Pts',(66.405188094332,-4.65875271127288,336.582394333471));
#31782=CARTESIAN_POINT('Ctrl Pts',(66.397422583283,-4.61110121217894,336.710826897597));
#31783=CARTESIAN_POINT('Ctrl Pts',(66.3896647717608,-4.56349695968512,336.839132120462));
#31784=CARTESIAN_POINT('Ctrl Pts',(66.3819069602386,-4.51048383082645,336.965582674482));
#31785=CARTESIAN_POINT('Ctrl Pts',(66.3741491487164,-4.45223178580728,337.08969260609));
#31786=CARTESIAN_POINT('Ctrl Pts',(66.3663971751934,-4.39402357729927,337.213709141038));
#31787=CARTESIAN_POINT('Ctrl Pts',(66.3586452016703,-4.3305844652939,337.335388207126));
#31788=CARTESIAN_POINT('Ctrl Pts',(66.3508932281473,-4.26213285323817,337.454262945132));
#31789=CARTESIAN_POINT('Ctrl Pts',(66.3431445375897,-4.19371023048078,337.573087339616));
#31790=CARTESIAN_POINT('Ctrl Pts',(66.3353958470321,-4.12027952441099,337.689109430114));
#31791=CARTESIAN_POINT('Ctrl Pts',(66.3276471564745,-4.04210539715163,337.801886332601));
#31792=CARTESIAN_POINT('Ctrl Pts',(66.3199000780966,-3.96394753467243,337.914639770912));
#31793=CARTESIAN_POINT('Ctrl Pts',(66.3121529997188,-3.88104843657232,338.024149043168));
#31794=CARTESIAN_POINT('Ctrl Pts',(66.3044059213409,-3.79371624689646,338.13000001606));
#31795=CARTESIAN_POINT('Ctrl Pts',(66.2966587780351,-3.70638332529279,338.235851876084));
#31796=CARTESIAN_POINT('Ctrl Pts',(66.2889116347293,-3.61461748676222,338.338045074088));
#31797=CARTESIAN_POINT('Ctrl Pts',(66.2811644914235,-3.51876707772084,338.436198672261));
#31798=CARTESIAN_POINT('Ctrl Pts',(66.2734156063954,-3.4228951194726,338.534374337447));
#31799=CARTESIAN_POINT('Ctrl Pts',(66.2656667213674,-3.32293703643878,338.628508316014));
#31800=CARTESIAN_POINT('Ctrl Pts',(66.2579178363393,-3.21927763380795,338.718256927508));
#31801=CARTESIAN_POINT('Ctrl Pts',(66.2501607265645,-3.11550820601595,338.808100799107));
#31802=CARTESIAN_POINT('Ctrl Pts',(66.2424036167898,-3.00802990681466,338.89354974923));
#31803=CARTESIAN_POINT('Ctrl Pts',(66.2346465070151,-2.89726062273687,338.974300434849));
#31804=CARTESIAN_POINT('Ctrl Pts',(66.2268852520889,-2.7864321470953,339.055094271052));
#31805=CARTESIAN_POINT('Ctrl Pts',(66.2191239971627,-2.67230950746492,339.131184623423));
#31806=CARTESIAN_POINT('Ctrl Pts',(66.2113627422365,-2.55533825437342,339.202312395365));
#31807=CARTESIAN_POINT('Ctrl Pts',(66.2035890718318,-2.43817988539798,339.273553948561));
#31808=CARTESIAN_POINT('Ctrl Pts',(66.1958154014272,-2.31816413938298,339.339816868807));
#31809=CARTESIAN_POINT('Ctrl Pts',(66.1880417310225,-2.19576055217275,339.400888394407));
#31810=CARTESIAN_POINT('Ctrl Pts',(66.1806299268455,-2.07905488139724,339.459117025796));
#31811=CARTESIAN_POINT('Ctrl Pts',(66.1732181226685,-1.96017893697345,339.512626586462));
#31812=CARTESIAN_POINT('Ctrl Pts',(66.1658063184915,-1.83955355003807,339.561274580536));
#31813=CARTESIAN_POINT('Ctrl Pts',(66.158031239713,-1.71301595356296,339.612306957714));
#31814=CARTESIAN_POINT('Ctrl Pts',(66.1502561609346,-1.5841532054684,339.658150430498));
#31815=CARTESIAN_POINT('Ctrl Pts',(66.1424810821562,-1.45342986835477,339.698587519699));
#31816=CARTESIAN_POINT('Ctrl Pts',(66.1347155711072,-1.32286739462962,339.738974848488));
#31817=CARTESIAN_POINT('Ctrl Pts',(66.1269500600581,-1.19044925732672,339.773968916648));
#31818=CARTESIAN_POINT('Ctrl Pts',(66.1191845490091,-1.05666061376249,339.803399984368));
#31819=CARTESIAN_POINT('Ctrl Pts',(66.1114267374869,-0.92300462202786,339.832801871098));
#31820=CARTESIAN_POINT('Ctrl Pts',(66.1036689259647,-0.787981207529575,
339.856651650567));
#31821=CARTESIAN_POINT('Ctrl Pts',(66.0959111144425,-0.65209099421004,339.874829268576));
#31822=CARTESIAN_POINT('Ctrl Pts',(66.0881591409195,-0.51630304258554,339.892993207352));
#31823=CARTESIAN_POINT('Ctrl Pts',(66.0804071673965,-0.379649976361819,
339.905493429256));
#31824=CARTESIAN_POINT('Ctrl Pts',(66.0726551938735,-0.242642578055625,
339.912260950094));
#31825=CARTESIAN_POINT('Ctrl Pts',(66.0649065033159,-0.105693202463863,
339.919025604882));
#31826=CARTESIAN_POINT('Ctrl Pts',(66.0571578127583,0.0316098171660805,
339.920062368087));
#31827=CARTESIAN_POINT('Ctrl Pts',(66.0494091222006,0.168750826347874,339.915354129776));
#31828=CARTESIAN_POINT('Ctrl Pts',(66.0416620438228,0.305863302197189,339.910646871053));
#31829=CARTESIAN_POINT('Ctrl Pts',(66.033914965445,0.442813444246325,339.900197001745));
#31830=CARTESIAN_POINT('Ctrl Pts',(66.0261678870671,0.579086244535765,339.884039535455));
#31831=CARTESIAN_POINT('Ctrl Pts',(66.0184207437613,0.715360186922433,339.86788193375));
#31832=CARTESIAN_POINT('Ctrl Pts',(66.0106736004556,0.850956388071212,339.846016685676));
#31833=CARTESIAN_POINT('Ctrl Pts',(66.0029264571498,0.98536599901788,339.818530575858));
#31834=CARTESIAN_POINT('Ctrl Pts',(65.9951775721216,1.11980582809887,339.791038286579));
#31835=CARTESIAN_POINT('Ctrl Pts',(65.9874286870936,1.25305815325959,339.757922699253));
#31836=CARTESIAN_POINT('Ctrl Pts',(65.9796798020655,1.38462572610689,339.719321419558));
#31837=CARTESIAN_POINT('Ctrl Pts',(65.9719226922907,1.51633294613527,339.680679168067));
#31838=CARTESIAN_POINT('Ctrl Pts',(65.964165582516,1.64635146606899,339.636539703291));
#31839=CARTESIAN_POINT('Ctrl Pts',(65.9564084727413,1.7742000559003,339.587090278613));
#31840=CARTESIAN_POINT('Ctrl Pts',(65.9486472178151,1.90211696393022,339.537614429743));
#31841=CARTESIAN_POINT('Ctrl Pts',(65.9408859628889,2.027861273215,339.48282312311));
#31842=CARTESIAN_POINT('Ctrl Pts',(65.9331247079628,2.15097399094221,339.422950819621));
#31843=CARTESIAN_POINT('Ctrl Pts',(65.9253510375581,2.27428364889544,339.36298273996));
#31844=CARTESIAN_POINT('Ctrl Pts',(65.9175773671534,2.39495295885802,339.297917607023));
#31845=CARTESIAN_POINT('Ctrl Pts',(65.9098036967488,2.51254891219449,339.228035125957));
#31846=CARTESIAN_POINT('Ctrl Pts',(65.9023918925717,2.62467074561071,339.161405691199));
#31847=CARTESIAN_POINT('Ctrl Pts',(65.8949800883947,2.73399867138034,339.09039746708));
#31848=CARTESIAN_POINT('Ctrl Pts',(65.8875682842176,2.84018512581103,339.01528722679));
#31849=CARTESIAN_POINT('Ctrl Pts',(65.8797932054392,2.95157609468705,338.936495609881));
#31850=CARTESIAN_POINT('Ctrl Pts',(65.8720181266607,3.05986187611574,338.852940709464));
#31851=CARTESIAN_POINT('Ctrl Pts',(65.8642430478823,3.16460818572794,338.764895495671));
#31852=CARTESIAN_POINT('Ctrl Pts',(65.8564775368333,3.26922559833768,338.676958627119));
#31853=CARTESIAN_POINT('Ctrl Pts',(65.8487120257843,3.37031190906547,338.584542688685));
#31854=CARTESIAN_POINT('Ctrl Pts',(65.8409465147353,3.46746183361833,338.487963803554));
#31855=CARTESIAN_POINT('Ctrl Pts',(65.8331887032131,3.56451543373815,338.391480676668));
#31856=CARTESIAN_POINT('Ctrl Pts',(65.8254308916908,3.65764013933336,338.290843090989));
#31857=CARTESIAN_POINT('Ctrl Pts',(65.8176730801686,3.74646407792625,338.186407063655));
#31858=CARTESIAN_POINT('Ctrl Pts',(65.8099211066456,3.83522117368845,338.082049627743));
#31859=CARTESIAN_POINT('Ctrl Pts',(65.8021691331226,3.91968369225314,337.973899736325));
#31860=CARTESIAN_POINT('Ctrl Pts',(65.7944171595996,3.99951720961025,337.86234958601));
#31861=CARTESIAN_POINT('Ctrl Pts',(65.786668469042,4.07931691742543,337.75084667725));
#31862=CARTESIAN_POINT('Ctrl Pts',(65.7789197784844,4.15449129609051,337.635946690871));
#31863=CARTESIAN_POINT('Ctrl Pts',(65.7711710879267,4.22474690726673,337.518073992567));
#31864=CARTESIAN_POINT('Ctrl Pts',(65.7634240095489,4.29498790117625,337.400225818661));
#31865=CARTESIAN_POINT('Ctrl Pts',(65.7556769311711,4.3603119631969,337.279406498613));
#31866=CARTESIAN_POINT('Ctrl Pts',(65.7479298527933,4.42046983665772,337.156068061472));
#31867=CARTESIAN_POINT('Ctrl Pts',(65.7401827094875,4.48062821429947,337.032728590636));
#31868=CARTESIAN_POINT('Ctrl Pts',(65.7324355661817,4.5356201456691,336.906870311911));
#31869=CARTESIAN_POINT('Ctrl Pts',(65.7246884228759,4.58524324243812,336.778968091388));
#31870=CARTESIAN_POINT('Ctrl Pts',(65.7169395378478,4.63487749553275,336.65103711573));
#31871=CARTESIAN_POINT('Ctrl Pts',(65.7091906528196,4.67914037082135,336.521061648214));
#31872=CARTESIAN_POINT('Ctrl Pts',(65.7014417677916,4.71787849421724,336.389534301952));
#31873=CARTESIAN_POINT('Ctrl Pts',(65.6936846580168,4.75665773465756,336.257867351206));
#31874=CARTESIAN_POINT('Ctrl Pts',(65.6859275482421,4.78990039865099,336.124645606858));
#31875=CARTESIAN_POINT('Ctrl Pts',(65.6781704384674,4.81750353038996,335.990375079038));
#31876=CARTESIAN_POINT('Ctrl Pts',(65.6704091835412,4.84512141235998,335.856032801341));
#31877=CARTESIAN_POINT('Ctrl Pts',(65.662647928615,4.86709369465182,335.720641009083));
#31878=CARTESIAN_POINT('Ctrl Pts',(65.6548866736888,4.88336915309756,335.584712559362));
#31879=CARTESIAN_POINT('Ctrl Pts',(65.6471130032842,4.89967064697264,335.44856666842));
#31880=CARTESIAN_POINT('Ctrl Pts',(65.6393393328796,4.91025707620642,335.311882794437));
#31881=CARTESIAN_POINT('Ctrl Pts',(65.6315656624749,4.91512932500585,335.175176428116));
#31882=CARTESIAN_POINT('Ctrl Pts',(65.6241538582978,4.9197747694515,335.044833776037));
#31883=CARTESIAN_POINT('Ctrl Pts',(65.6167420541206,4.91922605276479,334.914470966325));
#31884=CARTESIAN_POINT('Ctrl Pts',(65.6093302499435,4.91352783276819,334.784530050559));
#31885=CARTESIAN_POINT('Ctrl Pts',(65.6015551711651,4.90755032603547,334.648220343437));
#31886=CARTESIAN_POINT('Ctrl Pts',(65.5937800923866,4.89588687747655,334.511944168663));
#31887=CARTESIAN_POINT('Ctrl Pts',(65.5860050136082,4.87853201730905,334.376214445029));
#31888=CARTESIAN_POINT('Ctrl Pts',(65.5782395025592,4.86119851340186,334.240651745461));
#31889=CARTESIAN_POINT('Ctrl Pts',(65.5704739915102,4.83818758223108,334.105634543076));
#31890=CARTESIAN_POINT('Ctrl Pts',(65.5627084804612,4.80954573594088,333.971674722477));
#31891=CARTESIAN_POINT('Ctrl Pts',(65.554950668939,4.78093228812467,333.83784772343));
#31892=CARTESIAN_POINT('Ctrl Pts',(65.5471928574167,4.74669911701042,333.705076399572));
#31893=CARTESIAN_POINT('Ctrl Pts',(65.5394350458945,4.70694436346909,333.573866127705));
#31894=CARTESIAN_POINT('Ctrl Pts',(65.5316830723715,4.66721952664052,333.442754595729));
#31895=CARTESIAN_POINT('Ctrl Pts',(65.5239310988486,4.62198149092398,333.313202150053));
#31896=CARTESIAN_POINT('Ctrl Pts',(65.5161791253256,4.57137908679407,333.185702255052));
#31897=CARTESIAN_POINT('Ctrl Pts',(65.5084304347679,4.52079811281232,333.058256356333));
#31898=CARTESIAN_POINT('Ctrl Pts',(65.5006817442103,4.46485743278348,332.932861641949));
#31899=CARTESIAN_POINT('Ctrl Pts',(65.4929330536526,4.40375510854871,332.809994519087));
#31900=CARTESIAN_POINT('Ctrl Pts',(65.4851859752748,4.34266549716282,332.687152959755));
#31901=CARTESIAN_POINT('Ctrl Pts',(65.477438896897,4.27641655161998,332.566838295685));
#31902=CARTESIAN_POINT('Ctrl Pts',(65.4696918185192,4.20525350570571,332.449504750985));
#31903=CARTESIAN_POINT('Ctrl Pts',(65.4619446752134,4.13408986337662,332.332170222917));
#31904=CARTESIAN_POINT('Ctrl Pts',(65.4541975319075,4.05801224122849,332.217817198262));
#31905=CARTESIAN_POINT('Ctrl Pts',(65.4464503886017,3.97731044035036,332.106872846973));
#31906=CARTESIAN_POINT('Ctrl Pts',(65.4387015035736,3.89659049599416,331.995903553039));
#31907=CARTESIAN_POINT('Ctrl Pts',(65.4309526185455,3.81124453407735,331.888344773439));
#31908=CARTESIAN_POINT('Ctrl Pts',(65.4232037335174,3.72160380395527,331.784592064934));
#31909=CARTESIAN_POINT('Ctrl Pts',(65.4154466237427,3.63186792823594,331.680729232232));
#31910=CARTESIAN_POINT('Ctrl Pts',(65.407689513968,3.53782843420305,331.58068083675));
#31911=CARTESIAN_POINT('Ctrl Pts',(65.3999324041932,3.43985512127422,331.484807287339));
#31912=CARTESIAN_POINT('Ctrl Pts',(65.3921711492671,3.34182945453953,331.388882506169));
#31913=CARTESIAN_POINT('Ctrl Pts',(65.3844098943409,3.23986607068938,331.297137277661));
#31914=CARTESIAN_POINT('Ctrl Pts',(65.3766486394147,3.13436852186318,331.209892213716));
#31915=CARTESIAN_POINT('Ctrl Pts',(65.36887496901,3.02870221134042,331.122507586101));
#31916=CARTESIAN_POINT('Ctrl Pts',(65.3611012986054,2.91949074999282,331.039637744775));
#31917=CARTESIAN_POINT('Ctrl Pts',(65.3533276282007,2.80716810344607,330.961560907789));
#31918=CARTESIAN_POINT('Ctrl Pts',(65.3459158240237,2.70007410312047,330.88711856635));
#31919=CARTESIAN_POINT('Ctrl Pts',(65.3385040198467,2.59015229318238,330.817033197368));
#31920=CARTESIAN_POINT('Ctrl Pts',(65.3310922156697,2.47779857114452,330.751506466601));
#31921=CARTESIAN_POINT('Ctrl Pts',(65.3233171368912,2.35993805850395,330.682768075564));
#31922=CARTESIAN_POINT('Ctrl Pts',(65.3155420581128,2.23902875454784,330.618829260591));
#31923=CARTESIAN_POINT('Ctrl Pts',(65.3077669793344,2.11549902361918,330.559972191127));
#31924=CARTESIAN_POINT('Ctrl Pts',(65.3000014682854,1.9921213038887,330.501187549034));
#31925=CARTESIAN_POINT('Ctrl Pts',(65.2922359572364,1.86612992271413,330.447472376476));
#31926=CARTESIAN_POINT('Ctrl Pts',(65.2844704461873,1.73798050516856,330.39906457053));
#31927=CARTESIAN_POINT('Ctrl Pts',(65.2767126346652,1.60995814814376,330.350704761064));
#31928=CARTESIAN_POINT('Ctrl Pts',(65.2689548231429,1.47978237617114,330.30764198323));
#31929=CARTESIAN_POINT('Ctrl Pts',(65.2611970116207,1.34793128104159,330.270067196662));
#31930=CARTESIAN_POINT('Ctrl Pts',(65.2534450380977,1.21617940804218,330.232520686313));
#31931=CARTESIAN_POINT('Ctrl Pts',(65.2456930645747,1.08275509570918,330.200454053585));
#31932=CARTESIAN_POINT('Ctrl Pts',(65.2379410910517,0.948153849472003,330.174009185646));
#31933=CARTESIAN_POINT('Ctrl Pts',(65.2301924004941,0.813609606942613,330.147575517123));
#31934=CARTESIAN_POINT('Ctrl Pts',(65.2224437099365,0.677889804599434,330.126758953301));
#31935=CARTESIAN_POINT('Ctrl Pts',(65.2146950193789,0.541502246035292,330.111650751016));
#31936=CARTESIAN_POINT('Ctrl Pts',(65.206947941001,0.40514306404184,330.096545692119));
#31937=CARTESIAN_POINT('Ctrl Pts',(65.1992008626232,0.26811679042755,330.087146675403));
#31938=CARTESIAN_POINT('Ctrl Pts',(65.1914537842454,0.130938102009095,330.083493285274));
#31939=CARTESIAN_POINT('Ctrl Pts',(65.1837066409396,-0.00624173609880257,
330.079839864527));
#31940=CARTESIAN_POINT('Ctrl Pts',(65.1759594976338,-0.143573600822953,
330.08193217682));
#31941=CARTESIAN_POINT('Ctrl Pts',(65.168212354328,-0.280541447838741,330.089757688408));
#31942=CARTESIAN_POINT('Ctrl Pts',(65.1604634692999,-0.417540088134261,
330.097584959337));
#31943=CARTESIAN_POINT('Ctrl Pts',(65.1527145842718,-0.554174157709508,
330.111147972126));
#31944=CARTESIAN_POINT('Ctrl Pts',(65.1449656992437,-0.689931766411287,
330.130382230586));
#31945=CARTESIAN_POINT('Ctrl Pts',(65.137208589469,-0.825833469641766,330.149636904486));
#31946=CARTESIAN_POINT('Ctrl Pts',(65.1294514796943,-0.960856466047415,
330.174574793691));
#31947=CARTESIAN_POINT('Ctrl Pts',(65.1216943699196,-1.09449756045277,330.205079963893));
#31948=CARTESIAN_POINT('Ctrl Pts',(65.1139331149934,-1.22821006838595,330.235601435082));
#31949=CARTESIAN_POINT('Ctrl Pts',(65.1061718600672,-1.36053882599565,330.271696012369));
#31950=CARTESIAN_POINT('Ctrl Pts',(65.098410605141,-1.49099583867701,330.313197841646));
#31951=CARTESIAN_POINT('Ctrl Pts',(65.0906369347364,-1.62166154006283,330.354766060325));
#31952=CARTESIAN_POINT('Ctrl Pts',(65.0828632643318,-1.75044914587142,330.401758681885));
#31953=CARTESIAN_POINT('Ctrl Pts',(65.0750895939271,-1.87688985290771,330.453961335123));
#31954=CARTESIAN_POINT('Ctrl Pts',(65.06767778975,-1.99744471461211,330.503733942295));
#31955=CARTESIAN_POINT('Ctrl Pts',(65.0602659855729,-2.11586599526626,330.558242322697));
#31956=CARTESIAN_POINT('Ctrl Pts',(65.0528541813957,-2.23176986697115,330.61726269058));
#31957=CARTESIAN_POINT('Ctrl Pts',(65.0450791026173,-2.35335453268751,330.679175822505));
#31958=CARTESIAN_POINT('Ctrl Pts',(65.0373040238389,-2.47255300841858,330.746250074098));
#31959=CARTESIAN_POINT('Ctrl Pts',(65.0295289450605,-2.58889619933093,330.818277922723));
#31960=CARTESIAN_POINT('Ctrl Pts',(65.0217634340115,-2.70509622254001,330.890217136494));
#31961=CARTESIAN_POINT('Ctrl Pts',(65.0139979229625,-2.81844762284406,330.967097614784));
#31962=CARTESIAN_POINT('Ctrl Pts',(65.0062324119135,-2.9285037826456,331.048664952509));
#31963=CARTESIAN_POINT('Ctrl Pts',(64.9984746003913,-3.03845082144427,331.130151415981));
#31964=CARTESIAN_POINT('Ctrl Pts',(64.9907167888692,-3.14510880972732,331.216315259783));
#31965=CARTESIAN_POINT('Ctrl Pts',(64.982958977347,-3.24805844256378,331.306857785545));
#31966=CARTESIAN_POINT('Ctrl Pts',(64.975207003824,-3.35093060253687,331.397332175185));
#31967=CARTESIAN_POINT('Ctrl Pts',(64.9674550303009,-3.45009966939793,331.492178430956));
#31968=CARTESIAN_POINT('Ctrl Pts',(64.9597030567779,-3.54517818078163,331.59105665506));
#31969=CARTESIAN_POINT('Ctrl Pts',(64.9519543662203,-3.64021642635931,331.689893004177));
#31970=CARTESIAN_POINT('Ctrl Pts',(64.9442056756627,-3.73116729162761,331.792757644285));
#31971=CARTESIAN_POINT('Ctrl Pts',(64.9364569851051,-3.81767923510401,331.899272936817));
#31972=CARTESIAN_POINT('Ctrl Pts',(64.9287099067273,-3.90417317904801,332.005766067953));
#31973=CARTESIAN_POINT('Ctrl Pts',(64.9209628283495,-3.98622979194255,332.115908037502));
#31974=CARTESIAN_POINT('Ctrl Pts',(64.9132157499717,-4.06353726525788,332.229287464142));
#31975=CARTESIAN_POINT('Ctrl Pts',(64.9054686066659,-4.14084538648424,332.342667841011));
#31976=CARTESIAN_POINT('Ctrl Pts',(64.89772146336,-4.21340406854225,332.459285406143));
#31977=CARTESIAN_POINT('Ctrl Pts',(64.8899743200543,-4.28094459013163,332.578699424127));
#31978=CARTESIAN_POINT('Ctrl Pts',(64.8822254350262,-4.3485002962641,332.698140288918));
#31979=CARTESIAN_POINT('Ctrl Pts',(64.8744765499981,-4.41103540456437,332.820378517449));
#31980=CARTESIAN_POINT('Ctrl Pts',(64.86672766497,-4.46832713811948,332.944948747781));
#31981=CARTESIAN_POINT('Ctrl Pts',(64.8589705551953,-4.5256796817126,333.069651198244));
#31982=CARTESIAN_POINT('Ctrl Pts',(64.8512134454206,-4.57777756962596,333.196690239295));
#31983=CARTESIAN_POINT('Ctrl Pts',(64.8434563356459,-4.62444598571164,333.325579984671));
#31984=CARTESIAN_POINT('Ctrl Pts',(64.8356950807197,-4.67113933990671,333.454538604605));
#31985=CARTESIAN_POINT('Ctrl Pts',(64.8279338257936,-4.71239732358709,333.585349526865));
#31986=CARTESIAN_POINT('Ctrl Pts',(64.8201725708674,-4.7480953251286,333.717512633204));
#31987=CARTESIAN_POINT('Ctrl Pts',(64.8123989004627,-4.78385043183862,333.849887157441));
#31988=CARTESIAN_POINT('Ctrl Pts',(64.8046252300581,-4.81402769715993,333.98361780669));
#31989=CARTESIAN_POINT('Ctrl Pts',(64.7968515596534,-4.83855369410069,334.118194345786));
#31990=CARTESIAN_POINT('Ctrl Pts',(64.7894397554763,-4.86193799998361,334.246506314611));
#31991=CARTESIAN_POINT('Ctrl Pts',(64.7820279512991,-4.88018528999157,334.375586908248));
#31992=CARTESIAN_POINT('Ctrl Pts',(64.7746161471219,-4.89327603903691,334.504992254316));
#31993=CARTESIAN_POINT('Ctrl Pts',(64.7652561809112,-4.90980763725605,334.668411259691));
#31994=CARTESIAN_POINT('Ctrl Pts',(64.7558962147006,-4.91815464120901,334.832672048007));
#31995=CARTESIAN_POINT('Ctrl Pts',(64.7465362484901,-4.91824918766929,334.997173254461));
#31996=CARTESIAN_POINT('',(68.2465362484391,-4.91824996458591,335.000590212407));
#31997=CARTESIAN_POINT('Ctrl Pts',(68.2465362484391,-4.91824996458591,335.000590212407));
#31998=CARTESIAN_POINT('Ctrl Pts',(68.2383441378392,-4.91823250944352,335.146044209075));
#31999=CARTESIAN_POINT('Ctrl Pts',(68.2301520272394,-4.9117582215266,335.291349637273));
#32000=CARTESIAN_POINT('Ctrl Pts',(68.2219599166395,-4.89889212011513,335.435934694621));
#32001=CARTESIAN_POINT('Ctrl Pts',(68.2137541776497,-4.88600461466552,335.580760283577));
#32002=CARTESIAN_POINT('Ctrl Pts',(68.2055484386599,-4.86670409518988,335.724862792216));
#32003=CARTESIAN_POINT('Ctrl Pts',(68.19734269967,-4.84110687754105,335.867679239538));
#32004=CARTESIAN_POINT('Ctrl Pts',(68.1891149144263,-4.81544088817531,336.01087938998));
#32005=CARTESIAN_POINT('Ctrl Pts',(68.1808871291826,-4.78344442544275,336.15278625445));
#32006=CARTESIAN_POINT('Ctrl Pts',(68.1726593439388,-4.74528454118827,336.292848670827));
#32007=CARTESIAN_POINT('Ctrl Pts',(68.164419561526,-4.70706901491457,336.433115316222));
#32008=CARTESIAN_POINT('Ctrl Pts',(68.1561797791132,-4.66267222273283,336.571531841512));
#32009=CARTESIAN_POINT('Ctrl Pts',(68.1479399967003,-4.61230994494546,336.70756552854));
#32010=CARTESIAN_POINT('Ctrl Pts',(68.1396810005123,-4.56183023086696,336.843916423056));
#32011=CARTESIAN_POINT('Ctrl Pts',(68.1314220043242,-4.50535734070595,336.977873075394));
#32012=CARTESIAN_POINT('Ctrl Pts',(68.1231630081361,-4.44315446345079,337.108924246249));
#32013=CARTESIAN_POINT('Ctrl Pts',(68.1199328582271,-4.41882649262576,337.160179255693));
#32014=CARTESIAN_POINT('Ctrl Pts',(68.1167027083181,-4.39362251811818,337.210990123609));
#32015=CARTESIAN_POINT('Ctrl Pts',(68.113472558409,-4.36756010055526,337.261327448765));
#32016=CARTESIAN_POINT('Ctrl Pts',(68.1056974796306,-4.30482699050945,337.382491072622));
#32017=CARTESIAN_POINT('Ctrl Pts',(68.0979224008521,-4.23694899898551,337.501233693909));
#32018=CARTESIAN_POINT('Ctrl Pts',(68.0901473220737,-4.16413681295339,337.61708763046));
#32019=CARTESIAN_POINT('Ctrl Pts',(68.0823818110247,-4.09141422695164,337.732799001366));
#32020=CARTESIAN_POINT('Ctrl Pts',(68.0746162999757,-4.01376973366603,337.845628432614));
#32021=CARTESIAN_POINT('Ctrl Pts',(68.0668507889267,-3.93146074959675,337.955131035484));
#32022=CARTESIAN_POINT('Ctrl Pts',(68.0590929774045,-3.84923337512486,338.064525066204));
#32023=CARTESIAN_POINT('Ctrl Pts',(68.0513351658823,-3.76235094693859,338.170598522431));
#32024=CARTESIAN_POINT('Ctrl Pts',(68.0435773543601,-3.67111498929645,338.272934126722));
#32025=CARTESIAN_POINT('Ctrl Pts',(68.0358253808371,-3.57994768960564,338.375192720226));
#32026=CARTESIAN_POINT('Ctrl Pts',(68.0280734073141,-3.48443364057982,338.473718770054));
#32027=CARTESIAN_POINT('Ctrl Pts',(68.0203214337911,-3.38491534984609,338.568127118935));
#32028=CARTESIAN_POINT('Ctrl Pts',(68.0125727432335,-3.28543920516764,338.662495485823));
#32029=CARTESIAN_POINT('Ctrl Pts',(68.0048240526758,-3.1819624745896,338.752749351704));
#32030=CARTESIAN_POINT('Ctrl Pts',(67.9970753621182,-3.07486516297142,338.838539734332));
#32031=CARTESIAN_POINT('Ctrl Pts',(67.9893282837404,-2.96779013384341,338.924312267555));
#32032=CARTESIAN_POINT('Ctrl Pts',(67.9815812053626,-2.85709632690015,339.005622920487));
#32033=CARTESIAN_POINT('Ctrl Pts',(67.9738341269847,-2.74319722056397,339.082162670888));
#32034=CARTESIAN_POINT('Ctrl Pts',(67.9660869836789,-2.62929715964365,339.158703062766));
#32035=CARTESIAN_POINT('Ctrl Pts',(67.9583398403731,-2.51219207017602,339.230472254346));
#32036=CARTESIAN_POINT('Ctrl Pts',(67.9505926970673,-2.39232449291819,339.297204507943));
#32037=CARTESIAN_POINT('Ctrl Pts',(67.9428438120392,-2.27242996688413,339.363951764367));
#32038=CARTESIAN_POINT('Ctrl Pts',(67.9350949270111,-2.14977205865853,339.425659639345));
#32039=CARTESIAN_POINT('Ctrl Pts',(67.927346041983,-2.02481762457754,339.4821085049));
#32040=CARTESIAN_POINT('Ctrl Pts',(67.9195889322083,-1.89973056256911,339.538617285865));
#32041=CARTESIAN_POINT('Ctrl Pts',(67.9118318224336,-1.77234246223286,339.589855745728));
#32042=CARTESIAN_POINT('Ctrl Pts',(67.9040747126588,-1.64314037975421,339.635652354839));
#32043=CARTESIAN_POINT('Ctrl Pts',(67.8963134577327,-1.51386925581384,339.681473436193));
#32044=CARTESIAN_POINT('Ctrl Pts',(67.8885522028065,-1.38278259161438,339.721846757448));
#32045=CARTESIAN_POINT('Ctrl Pts',(67.8807909478804,-1.2503813358319,339.756651088476));
#32046=CARTESIAN_POINT('Ctrl Pts',(67.8730172774757,-1.11776828118954,339.791511095092));
#32047=CARTESIAN_POINT('Ctrl Pts',(67.865243607071,-0.983836814771475,339.820784226016));
#32048=CARTESIAN_POINT('Ctrl Pts',(67.8574699366664,-0.849097656151765,
339.844400502933));
#32049=CARTESIAN_POINT('Ctrl Pts',(67.8500581324893,-0.720630637782078,
339.866917436478));
#32050=CARTESIAN_POINT('Ctrl Pts',(67.8426463283122,-0.591429716341078,
339.884292278768));
#32051=CARTESIAN_POINT('Ctrl Pts',(67.8352345241351,-0.461938885985191,
339.896508503834));
#32052=CARTESIAN_POINT('Ctrl Pts',(67.8274594453566,-0.326101324300288,
339.90932348248));
#32053=CARTESIAN_POINT('Ctrl Pts',(67.8196843665782,-0.189515444745477,
339.916501877123));
#32054=CARTESIAN_POINT('Ctrl Pts',(67.8119092877997,-0.0526885460399227,
339.917967769274));
#32055=CARTESIAN_POINT('Ctrl Pts',(67.8041437767507,0.0839699784559471,
339.919431857551));
#32056=CARTESIAN_POINT('Ctrl Pts',(67.7963782657017,0.220868544859206,339.915197426074));
#32057=CARTESIAN_POINT('Ctrl Pts',(67.7886127546527,0.357493733916682,339.905240187056));
#32058=CARTESIAN_POINT('Ctrl Pts',(67.7808549431305,0.493983458701527,339.89529282067));
#32059=CARTESIAN_POINT('Ctrl Pts',(67.7730971316083,0.630199958225146,339.87963396691));
#32060=CARTESIAN_POINT('Ctrl Pts',(67.7653393200861,0.765629162906398,339.858291371193));
#32061=CARTESIAN_POINT('Ctrl Pts',(67.7575873465631,0.900956452816237,339.836964836455));
#32062=CARTESIAN_POINT('Ctrl Pts',(67.7498353730401,1.03549724260055,339.809963133912));
#32063=CARTESIAN_POINT('Ctrl Pts',(67.7420833995171,1.16874229476243,339.777365854834));
#32064=CARTESIAN_POINT('Ctrl Pts',(67.7343347089595,1.30193091756562,339.744782380723));
#32065=CARTESIAN_POINT('Ctrl Pts',(67.7265860184018,1.43382451527536,339.706608135994));
#32066=CARTESIAN_POINT('Ctrl Pts',(67.7188373278442,1.56392397884424,339.662973820524));
#32067=CARTESIAN_POINT('Ctrl Pts',(67.7110902494664,1.69399637413319,339.619348583539));
#32068=CARTESIAN_POINT('Ctrl Pts',(67.7033431710885,1.822275007417,339.570265659637));
#32069=CARTESIAN_POINT('Ctrl Pts',(67.6955960927107,1.94827625840118,339.51590552198));
#32070=CARTESIAN_POINT('Ctrl Pts',(67.6878489494049,2.07427856539712,339.461544928733));
#32071=CARTESIAN_POINT('Ctrl Pts',(67.6801018060991,2.19800309312541,339.401907188351));
#32072=CARTESIAN_POINT('Ctrl Pts',(67.6723546627933,2.3189868928995,339.33722063689));
#32073=CARTESIAN_POINT('Ctrl Pts',(67.6646057777652,2.43999789240033,339.272519542518));
#32074=CARTESIAN_POINT('Ctrl Pts',(67.6568568927371,2.55826659319983,339.202767562647));
#32075=CARTESIAN_POINT('Ctrl Pts',(67.649108007709,2.67335566269407,339.128238433429));
#32076=CARTESIAN_POINT('Ctrl Pts',(67.6413508979342,2.78856688891576,339.053630198224));
#32077=CARTESIAN_POINT('Ctrl Pts',(67.6335937881595,2.90059141355886,338.974234897639));
#32078=CARTESIAN_POINT('Ctrl Pts',(67.6258366783848,3.00902141963126,338.890369283076));
#32079=CARTESIAN_POINT('Ctrl Pts',(67.6180754234586,3.11750936723192,338.80645885341));
#32080=CARTESIAN_POINT('Ctrl Pts',(67.6103141685325,3.22239867015139,338.718073601625));
#32081=CARTESIAN_POINT('Ctrl Pts',(67.6025529136063,3.3233162913176,338.625569181572));
#32082=CARTESIAN_POINT('Ctrl Pts',(67.5947792432016,3.4243953477887,338.532916784594));
#32083=CARTESIAN_POINT('Ctrl Pts',(67.587005572797,3.52148974956198,338.436132328015));
#32084=CARTESIAN_POINT('Ctrl Pts',(67.5792319023923,3.61426427071333,338.33560741754));
#32085=CARTESIAN_POINT('Ctrl Pts',(67.5718200982153,3.70272011558394,338.239761965832));
#32086=CARTESIAN_POINT('Ctrl Pts',(67.5644082940383,3.78724902327938,338.140516678744));
#32087=CARTESIAN_POINT('Ctrl Pts',(67.5569964898613,3.86759682604606,338.038235977283));
#32088=CARTESIAN_POINT('Ctrl Pts',(67.5492214110828,3.95188271397092,337.930942193964));
#32089=CARTESIAN_POINT('Ctrl Pts',(67.5414463323044,4.03183363589342,337.819968855152));
#32090=CARTESIAN_POINT('Ctrl Pts',(67.533671253526,4.10711122189202,337.705701475313));
#32091=CARTESIAN_POINT('Ctrl Pts',(67.525905742477,4.18229617402865,337.591574708759));
#32092=CARTESIAN_POINT('Ctrl Pts',(67.518140231428,4.2528190197808,337.474162289823));
#32093=CARTESIAN_POINT('Ctrl Pts',(67.510374720379,4.3183814944129,337.353882820196));
#32094=CARTESIAN_POINT('Ctrl Pts',(67.5026169088568,4.38387896366047,337.233722608012));
#32095=CARTESIAN_POINT('Ctrl Pts',(67.4948590973346,4.44442566346064,337.110701343238));
#32096=CARTESIAN_POINT('Ctrl Pts',(67.4871012858124,4.49976673297661,336.985266332585));
#32097=CARTESIAN_POINT('Ctrl Pts',(67.4793493122893,4.55506615658283,336.859925715756));
#32098=CARTESIAN_POINT('Ctrl Pts',(67.4715973387663,4.60516759015947,336.732175324721));
#32099=CARTESIAN_POINT('Ctrl Pts',(67.4638453652433,4.64986238607439,336.602486459559));
#32100=CARTESIAN_POINT('Ctrl Pts',(67.4560966746857,4.6945382537167,336.472852517708));
#32101=CARTESIAN_POINT('Ctrl Pts',(67.4483479841281,4.73381191068625,336.341282103307));
#32102=CARTESIAN_POINT('Ctrl Pts',(67.4405992935705,4.76752316875362,336.208265657005));
#32103=CARTESIAN_POINT('Ctrl Pts',(67.4328522151926,4.80122741291215,336.075276885885));
#32104=CARTESIAN_POINT('Ctrl Pts',(67.4251051368148,4.82937146416139,335.940843059952));
#32105=CARTESIAN_POINT('Ctrl Pts',(67.417358058437,4.85184537154071,335.80546853021));
#32106=CARTESIAN_POINT('Ctrl Pts',(67.4096109151312,4.87431946727301,335.6700928659));
#32107=CARTESIAN_POINT('Ctrl Pts',(67.4018637718254,4.89112326033665,335.533776867653));
#32108=CARTESIAN_POINT('Ctrl Pts',(67.3941166285196,4.9021982352922,335.397033404638));
#32109=CARTESIAN_POINT('Ctrl Pts',(67.3863677434915,4.91327570013724,335.260259198788));
#32110=CARTESIAN_POINT('Ctrl Pts',(67.3786188584634,4.91862175243003,335.123057726458));
#32111=CARTESIAN_POINT('Ctrl Pts',(67.3708699734353,4.91822991697447,334.985944884303));
#32112=CARTESIAN_POINT('Ctrl Pts',(67.3631128636606,4.91783766562072,334.84868650916));
#32113=CARTESIAN_POINT('Ctrl Pts',(67.3553557538858,4.911695361785,334.711517343602));
#32114=CARTESIAN_POINT('Ctrl Pts',(67.3475986441111,4.8998486753028,334.574951741995));
#32115=CARTESIAN_POINT('Ctrl Pts',(67.339837389185,4.88799565833015,334.438313164097));
#32116=CARTESIAN_POINT('Ctrl Pts',(67.3320761342588,4.87043223484404,334.302279180271));
#32117=CARTESIAN_POINT('Ctrl Pts',(67.3243148793326,4.84725560999143,334.167355950056));
#32118=CARTESIAN_POINT('Ctrl Pts',(67.316541208928,4.82404191009229,334.032216886645));
#32119=CARTESIAN_POINT('Ctrl Pts',(67.3087675385233,4.79519714782457,333.898192509829));
#32120=CARTESIAN_POINT('Ctrl Pts',(67.3009938681187,4.76086922279677,333.765776638559));
#32121=CARTESIAN_POINT('Ctrl Pts',(67.2935820639415,4.72813927093746,333.639524757952));
#32122=CARTESIAN_POINT('Ctrl Pts',(67.2861702597643,4.69042523394044,333.514735276587));
#32123=CARTESIAN_POINT('Ctrl Pts',(67.2787584555871,4.64789601645093,333.391819138666));
#32124=CARTESIAN_POINT('Ctrl Pts',(67.2709833768087,4.60328231532474,333.26287851468));
#32125=CARTESIAN_POINT('Ctrl Pts',(67.2632082980302,4.55322849864028,333.135592037477));
#32126=CARTESIAN_POINT('Ctrl Pts',(67.2554332192518,4.4978756423563,333.010452873542));
#32127=CARTESIAN_POINT('Ctrl Pts',(67.2476677082028,4.44259090128592,332.885467701315));
#32128=CARTESIAN_POINT('Ctrl Pts',(67.2399021971538,4.38202025175566,332.762624938774));
#32129=CARTESIAN_POINT('Ctrl Pts',(67.2321366861048,4.31635429669298,332.642401932491));
#32130=CARTESIAN_POINT('Ctrl Pts',(67.2243788745826,4.25075344961588,332.52229812767));
#32131=CARTESIAN_POINT('Ctrl Pts',(67.2166210630604,4.18006753695382,332.404809250772));
#32132=CARTESIAN_POINT('Ctrl Pts',(67.2088632515382,4.10453478864253,332.290391683043));
#32133=CARTESIAN_POINT('Ctrl Pts',(67.2011112780151,4.02905888111973,332.176060218162));
#32134=CARTESIAN_POINT('Ctrl Pts',(67.1933593044921,3.94874361239123,332.064795786895));
#32135=CARTESIAN_POINT('Ctrl Pts',(67.1856073309691,3.86387239754204,331.957028893004));
#32136=CARTESIAN_POINT('Ctrl Pts',(67.1778586404115,3.77903712570267,331.849307638456));
#32137=CARTESIAN_POINT('Ctrl Pts',(67.1701099498539,3.68964998660911,331.745081281703));
#32138=CARTESIAN_POINT('Ctrl Pts',(67.1623612592962,3.5960367152237,331.644749934019));
#32139=CARTESIAN_POINT('Ctrl Pts',(67.1546141809184,3.50244292086127,331.544439461111));
#32140=CARTESIAN_POINT('Ctrl Pts',(67.1468671025406,3.40462500964993,331.448022670965));
#32141=CARTESIAN_POINT('Ctrl Pts',(67.1391200241627,3.30294760033661,331.355864956957));
#32142=CARTESIAN_POINT('Ctrl Pts',(67.1313728808569,3.20126933886874,331.26370647058));
#32143=CARTESIAN_POINT('Ctrl Pts',(67.1236257375511,3.09573180439669,331.175807394038));
#32144=CARTESIAN_POINT('Ctrl Pts',(67.1158785942453,2.98673461348322,331.092494477148));
#32145=CARTESIAN_POINT('Ctrl Pts',(67.1081297092172,2.87771291768715,331.009162829745));
#32146=CARTESIAN_POINT('Ctrl Pts',(67.1003808241891,2.76523032819159,330.930419631022));
#32147=CARTESIAN_POINT('Ctrl Pts',(67.092631939161,2.64971716940016,330.856549507393));
#32148=CARTESIAN_POINT('Ctrl Pts',(67.0848748293863,2.53408140374851,330.782600977251));
#32149=CARTESIAN_POINT('Ctrl Pts',(67.0771177196115,2.41540897300358,330.713536065338));
#32150=CARTESIAN_POINT('Ctrl Pts',(67.0693606098368,2.29415712329452,330.649594713577));
#32151=CARTESIAN_POINT('Ctrl Pts',(67.0615993549106,2.17284048047385,330.585619193602));
#32152=CARTESIAN_POINT('Ctrl Pts',(67.0538380999844,2.04894202507939,330.526772856834));
#32153=CARTESIAN_POINT('Ctrl Pts',(67.0460768450583,1.92294000074851,330.473247873362));
#32154=CARTESIAN_POINT('Ctrl Pts',(67.0383031746536,1.79673641424266,330.41963726736));
#32155=CARTESIAN_POINT('Ctrl Pts',(67.030529504249,1.66842290051878,330.371365162715));
#32156=CARTESIAN_POINT('Ctrl Pts',(67.0227558338443,1.53849475943024,330.32857442126));
#32157=CARTESIAN_POINT('Ctrl Pts',(67.0153440296673,1.41461480456986,330.287775599115));
#32158=CARTESIAN_POINT('Ctrl Pts',(67.0079322254903,1.28926743797538,330.251959388634));
#32159=CARTESIAN_POINT('Ctrl Pts',(67.0005204213133,1.16288963539091,330.221206139788));
#32160=CARTESIAN_POINT('Ctrl Pts',(66.9927453425348,1.03031768024012,330.188945582606));
#32161=CARTESIAN_POINT('Ctrl Pts',(66.9849702637564,0.896192773727019,330.162154888396));
#32162=CARTESIAN_POINT('Ctrl Pts',(66.977195184978,0.761005974365572,330.140982304058));
#32163=CARTESIAN_POINT('Ctrl Pts',(66.969429673929,0.625985530967246,330.119835773932));
#32164=CARTESIAN_POINT('Ctrl Pts',(66.9616641628799,0.48990617720738,330.104293657813));
#32165=CARTESIAN_POINT('Ctrl Pts',(66.9538986518309,0.353272470183254,330.094453993253));
#32166=CARTESIAN_POINT('Ctrl Pts',(66.9461408403087,0.216774235877347,330.084624084749));
#32167=CARTESIAN_POINT('Ctrl Pts',(66.9383830287865,0.0797231294808181,
330.080485403925));
#32168=CARTESIAN_POINT('Ctrl Pts',(66.9306252172643,-0.0573681483938241,
330.082084592223));
#32169=CARTESIAN_POINT('Ctrl Pts',(66.9228732437413,-0.194356260734451,
330.083682577082));
#32170=CARTESIAN_POINT('Ctrl Pts',(66.9151212702183,-0.33138409510728,330.091009831896));
#32171=CARTESIAN_POINT('Ctrl Pts',(66.9073692966953,-0.46793625955047,330.104060997163));
#32172=CARTESIAN_POINT('Ctrl Pts',(66.8996206061377,-0.604430594070853,
330.117106635254));
#32173=CARTESIAN_POINT('Ctrl Pts',(66.8918719155801,-0.740449271033134,
330.135871325362));
#32174=CARTESIAN_POINT('Ctrl Pts',(66.8841232250225,-0.875479554450303,
330.160297673179));
#32175=CARTESIAN_POINT('Ctrl Pts',(66.8763761466446,-1.01048174368921,330.18471893889));
#32176=CARTESIAN_POINT('Ctrl Pts',(66.8686290682668,-1.14449556403225,330.214799449738));
#32177=CARTESIAN_POINT('Ctrl Pts',(66.860881989889,-1.27701643226724,330.250430325364));
#32178=CARTESIAN_POINT('Ctrl Pts',(66.8531348465832,-1.40953841115466,330.286061499611));
#32179=CARTESIAN_POINT('Ctrl Pts',(66.8453877032774,-1.54056703550862,330.327243029928));
#32180=CARTESIAN_POINT('Ctrl Pts',(66.8376405599716,-1.66961127898546,330.373815693297));
#32181=CARTESIAN_POINT('Ctrl Pts',(66.8298916749435,-1.79868453434784,330.420398827189));
#32182=CARTESIAN_POINT('Ctrl Pts',(66.8221427899154,-1.92577215349164,330.472375373294));
#32183=CARTESIAN_POINT('Ctrl Pts',(66.8143939048873,-2.05040191476713,330.529537490324));
#32184=CARTESIAN_POINT('Ctrl Pts',(66.8066367951126,-2.17516395935908,330.586760279816));
#32185=CARTESIAN_POINT('Ctrl Pts',(66.7988796853378,-2.29746257892062,330.649179471814));
#32186=CARTESIAN_POINT('Ctrl Pts',(66.7911225755631,-2.41684855905274,330.716540404637));
#32187=CARTESIAN_POINT('Ctrl Pts',(66.7833613206369,-2.53629833523533,330.783937332989));
#32188=CARTESIAN_POINT('Ctrl Pts',(66.7756000657108,-2.65283203876058,330.856281057961));
#32189=CARTESIAN_POINT('Ctrl Pts',(66.7678388107846,-2.76602926462784,330.933273408536));
#32190=CARTESIAN_POINT('Ctrl Pts',(66.76006514038,-2.87940756916561,331.01038892178));
#32191=CARTESIAN_POINT('Ctrl Pts',(66.7522914699753,-2.98943841670535,331.092167687243));
#32192=CARTESIAN_POINT('Ctrl Pts',(66.7445177995706,-3.09573363651364,331.178270507446));
#32193=CARTESIAN_POINT('Ctrl Pts',(66.7371059953935,-3.19708078826693,331.260365220653));
#32194=CARTESIAN_POINT('Ctrl Pts',(66.7296941912164,-3.29503205626142,331.346390288768));
#32195=CARTESIAN_POINT('Ctrl Pts',(66.7222823870393,-3.38928339984472,331.436021731543));
#32196=CARTESIAN_POINT('Ctrl Pts',(66.7146216124402,-3.48670074676993,331.528663990255));
#32197=CARTESIAN_POINT('Ctrl Pts',(66.706960837841,-3.58049266797326,331.625470871143));
#32198=CARTESIAN_POINT('Ctrl Pts',(66.6993000632418,-3.67027405721862,331.726122878389));
#32199=CARTESIAN_POINT('Ctrl Pts',(66.6916488412757,-3.75994349320634,331.826649377218));
#32200=CARTESIAN_POINT('Ctrl Pts',(66.6839976193096,-3.84561207674849,331.931011169319));
#32201=CARTESIAN_POINT('Ctrl Pts',(66.6763463973436,-3.9269291249062,332.038849765638));
#32202=CARTESIAN_POINT('Ctrl Pts',(66.6687038397904,-4.00815408784147,332.146566243147));
#32203=CARTESIAN_POINT('Ctrl Pts',(66.6610612822372,-4.0850370824608,332.257751368257));
#32204=CARTESIAN_POINT('Ctrl Pts',(66.6534187246839,-4.15726603818599,332.372011767483));
#32205=CARTESIAN_POINT('Ctrl Pts',(66.6457810204546,-4.22944912569078,332.486199606874));
#32206=CARTESIAN_POINT('Ctrl Pts',(66.6381433162252,-4.29698383526736,332.603458498373));
#32207=CARTESIAN_POINT('Ctrl Pts',(66.6305056119959,-4.35960007431012,332.723364268361));
#32208=CARTESIAN_POINT('Ctrl Pts',(66.6228709912686,-4.4221910338584,332.843221629864));
#32209=CARTESIAN_POINT('Ctrl Pts',(66.6152363705412,-4.4798672853151,332.96572338788));
#32210=CARTESIAN_POINT('Ctrl Pts',(66.6076017498139,-4.53240385282728,333.090419318966));
#32211=CARTESIAN_POINT('Ctrl Pts',(66.5999684456413,-4.58493136065385,333.215093746822));
#32212=CARTESIAN_POINT('Ctrl Pts',(66.5923351414687,-4.6323207920059,333.341961223155));
#32213=CARTESIAN_POINT('Ctrl Pts',(66.584701837296,-4.67439487409207,333.47055054887));
#32214=CARTESIAN_POINT('Ctrl Pts',(66.5770649754741,-4.71648856561941,333.599199806132));
#32215=CARTESIAN_POINT('Ctrl Pts',(66.5694281136522,-4.75326182912498,333.729572133486));
#32216=CARTESIAN_POINT('Ctrl Pts',(66.5617912518302,-4.78458694957643,333.861180091304));
#32217=CARTESIAN_POINT('Ctrl Pts',(66.5541527205776,-4.8159189177513,333.99281681884));
#32218=CARTESIAN_POINT('Ctrl Pts',(66.546514189325,-4.84180028910966,334.125689319563));
#32219=CARTESIAN_POINT('Ctrl Pts',(66.5388756580723,-4.86215453878236,334.259300125896));
#32220=CARTESIAN_POINT('Ctrl Pts',(66.5312289651637,-4.88253053666523,334.393053693369));
#32221=CARTESIAN_POINT('Ctrl Pts',(66.5235822722552,-4.89736756682387,334.527546741511));
#32222=CARTESIAN_POINT('Ctrl Pts',(66.5159355793466,-4.90664099949656,334.66227649688));
#32223=CARTESIAN_POINT('Ctrl Pts',(66.5094691357399,-4.91448309936048,334.776211027226));
#32224=CARTESIAN_POINT('Ctrl Pts',(66.5030026921332,-4.91834741662029,334.89031464222));
#32225=CARTESIAN_POINT('Ctrl Pts',(66.4965362485266,-4.91824813384112,335.00428444493));
#32226=CARTESIAN_POINT('',(69.9965362484408,-4.9182479192268,334.995475895536));
#32227=CARTESIAN_POINT('Ctrl Pts',(69.9965362484408,-4.9182479192268,334.995475895536));
#32228=CARTESIAN_POINT('Ctrl Pts',(69.9888786876184,-4.91837226176216,335.130651248063));
#32229=CARTESIAN_POINT('Ctrl Pts',(69.9812211267961,-4.91291958376056,335.265984642031));
#32230=CARTESIAN_POINT('Ctrl Pts',(69.9735635659737,-4.90187762434903,335.400972341199));
#32231=CARTESIAN_POINT('Ctrl Pts',(69.9656192825603,-4.89042222007096,335.541014394325));
#32232=CARTESIAN_POINT('Ctrl Pts',(69.9576749991469,-4.87295076806222,335.680683923758));
#32233=CARTESIAN_POINT('Ctrl Pts',(69.9497307157336,-4.84950892526431,335.819418236484));
#32234=CARTESIAN_POINT('Ctrl Pts',(69.9420814518508,-4.82693762057524,335.953000500913));
#32235=CARTESIAN_POINT('Ctrl Pts',(69.934432187968,-4.79883150560313,336.085715334998));
#32236=CARTESIAN_POINT('Ctrl Pts',(69.9267829240852,-4.76528407550447,336.217066449395));
#32237=CARTESIAN_POINT('Ctrl Pts',(69.919134721278,-4.73174129897208,336.348399343287));
#32238=CARTESIAN_POINT('Ctrl Pts',(69.9114865184707,-4.69275880747613,336.478368504336));
#32239=CARTESIAN_POINT('Ctrl Pts',(69.9038383156634,-4.64848079770478,336.606489755918));
#32240=CARTESIAN_POINT('Ctrl Pts',(69.8961894173898,-4.6041987616455,336.734622657822));
#32241=CARTESIAN_POINT('Ctrl Pts',(69.8885405191162,-4.55462038131386,336.860906936359));
#32242=CARTESIAN_POINT('Ctrl Pts',(69.8808916208425,-4.49993893860682,336.984875968747));
#32243=CARTESIAN_POINT('Ctrl Pts',(69.873240270243,-4.44523996439255,337.108884747051));
#32244=CARTESIAN_POINT('Ctrl Pts',(69.8655889196436,-4.38543483662483,337.230576435766));
#32245=CARTESIAN_POINT('Ctrl Pts',(69.8579375690441,-4.3207637078602,337.349507191591));
#32246=CARTESIAN_POINT('Ctrl Pts',(69.8502779279927,-4.25602250612296,337.468566812209));
#32247=CARTESIAN_POINT('Ctrl Pts',(69.8426182869414,-4.18640497263787,337.584859176312));
#32248=CARTESIAN_POINT('Ctrl Pts',(69.83495864589,-4.11219581219732,337.697967506225));
#32249=CARTESIAN_POINT('Ctrl Pts',(69.827294070046,-4.03793884183712,337.811148707199));
#32250=CARTESIAN_POINT('Ctrl Pts',(69.8196294942019,-3.95908458950933,337.921141465313));
#32251=CARTESIAN_POINT('Ctrl Pts',(69.8119649183578,-3.87595847820086,338.027561549789));
#32252=CARTESIAN_POINT('Ctrl Pts',(69.8042896202234,-3.79271607835604,338.134130509699));
#32253=CARTESIAN_POINT('Ctrl Pts',(69.7966143220889,-3.70519015408199,338.237116518811));
#32254=CARTESIAN_POINT('Ctrl Pts',(69.7889390239544,-3.61374357270736,338.336171526348));
#32255=CARTESIAN_POINT('Ctrl Pts',(69.7869262706539,-3.58976282234917,338.362147493648));
#32256=CARTESIAN_POINT('Ctrl Pts',(69.7849135173533,-3.56551263235681,338.387853344704));
#32257=CARTESIAN_POINT('Ctrl Pts',(69.7829007640527,-3.54099991569648,338.413283266818));
#32258=CARTESIAN_POINT('Ctrl Pts',(69.7751256852743,-3.44630957135392,338.511516690511));
#32259=CARTESIAN_POINT('Ctrl Pts',(69.7673506064958,-3.34737875468833,338.605962046973));
#32260=CARTESIAN_POINT('Ctrl Pts',(69.7595755277174,-3.24454281224072,338.696231188932));
#32261=CARTESIAN_POINT('Ctrl Pts',(69.7518100166684,-3.14183341596715,338.786389248966));
#32262=CARTESIAN_POINT('Ctrl Pts',(69.7440445056194,-3.03522874643746,338.872381064435));
#32263=CARTESIAN_POINT('Ctrl Pts',(69.7362789945704,-2.92510243582782,338.95385366477));
#32264=CARTESIAN_POINT('Ctrl Pts',(69.7285211830482,-2.81508531577622,339.035245484784));
#32265=CARTESIAN_POINT('Ctrl Pts',(69.720763371526,-2.70155381556513,339.112126775767));
#32266=CARTESIAN_POINT('Ctrl Pts',(69.7130055600039,-2.58491596580884,339.184183613587));
#32267=CARTESIAN_POINT('Ctrl Pts',(69.7052535864809,-2.46836588973304,339.256186226351));
#32268=CARTESIAN_POINT('Ctrl Pts',(69.6975016129579,-2.34871444823933,339.323371407786));
#32269=CARTESIAN_POINT('Ctrl Pts',(69.6897496394349,-2.22639978957823,339.385467710458));
#32270=CARTESIAN_POINT('Ctrl Pts',(69.6820009488772,-2.1041369312476,339.447537715308));
#32271=CARTESIAN_POINT('Ctrl Pts',(69.6742522583196,-1.97921344681806,339.50452295125));
#32272=CARTESIAN_POINT('Ctrl Pts',(69.666503567762,-1.85209310418054,339.556197339443));
#32273=CARTESIAN_POINT('Ctrl Pts',(69.6587564893841,-1.72499920999185,339.607860976347));
#32274=CARTESIAN_POINT('Ctrl Pts',(69.6510094110063,-1.59570972862215,339.654215816257));
#32275=CARTESIAN_POINT('Ctrl Pts',(69.6432623326285,-1.46470911139812,339.695083628807));
#32276=CARTESIAN_POINT('Ctrl Pts',(69.6355151893227,-1.33370739626284,339.735951783868));
#32277=CARTESIAN_POINT('Ctrl Pts',(69.6277680460169,-1.20099488980739,339.771332703439));
#32278=CARTESIAN_POINT('Ctrl Pts',(69.620020902711,-1.0670715504776,339.801097933667));
#32279=CARTESIAN_POINT('Ctrl Pts',(69.6122720176829,-0.933118102338027,
339.830869855751));
#32280=CARTESIAN_POINT('Ctrl Pts',(69.6045231326549,-0.797953661124003,
339.855023491418));
#32281=CARTESIAN_POINT('Ctrl Pts',(69.5967742476268,-0.662088336959024,
339.873481517002));
#32282=CARTESIAN_POINT('Ctrl Pts',(69.5890171378521,-0.526078803935131,
339.891959134126));
#32283=CARTESIAN_POINT('Ctrl Pts',(69.5812600280773,-0.389367289829594,
339.904729012253));
#32284=CARTESIAN_POINT('Ctrl Pts',(69.5735029183026,-0.252469544443574,
339.911765689813));
#32285=CARTESIAN_POINT('Ctrl Pts',(69.5657416633764,-0.115498645279374,
339.91880612755));
#32286=CARTESIAN_POINT('Ctrl Pts',(69.5579804084502,0.0216582928015551,
339.920107256437));
#32287=CARTESIAN_POINT('Ctrl Pts',(69.550219153524,0.158486553525184,339.91569578746));
#32288=CARTESIAN_POINT('Ctrl Pts',(69.5424454831194,0.295533694873559,339.91127726157));
#32289=CARTESIAN_POINT('Ctrl Pts',(69.5346718127147,0.432250718200474,339.901127905749));
#32290=CARTESIAN_POINT('Ctrl Pts',(69.5268981423101,0.568128162747628,339.885326340501));
#32291=CARTESIAN_POINT('Ctrl Pts',(69.5194863381329,0.697680479561715,339.870260341916));
#32292=CARTESIAN_POINT('Ctrl Pts',(69.5120745339558,0.826469339011665,339.850056556936));
#32293=CARTESIAN_POINT('Ctrl Pts',(69.5046627297787,0.954064481356156,339.824825802857));
#32294=CARTESIAN_POINT('Ctrl Pts',(69.4968876510003,1.08791344171287,339.798358414362));
#32295=CARTESIAN_POINT('Ctrl Pts',(69.4891125722218,1.22087169841239,339.766275181687));
#32296=CARTESIAN_POINT('Ctrl Pts',(69.4813374934434,1.35243137487755,339.728648056131));
#32297=CARTESIAN_POINT('Ctrl Pts',(69.4735719823944,1.48382915878506,339.691067233148));
#32298=CARTESIAN_POINT('Ctrl Pts',(69.4658064713453,1.61383141462508,339.647956197789));
#32299=CARTESIAN_POINT('Ctrl Pts',(69.4580409602963,1.74193912810579,339.599438132693));
#32300=CARTESIAN_POINT('Ctrl Pts',(69.4502831487741,1.86991982241595,339.550968173401));
#32301=CARTESIAN_POINT('Ctrl Pts',(69.4425253372519,1.99600934939483,339.497101990783));
#32302=CARTESIAN_POINT('Ctrl Pts',(69.4347675257296,2.11972291476512,339.438012824127));
#32303=CARTESIAN_POINT('Ctrl Pts',(69.4270155522066,2.24334338175396,339.378968123944));
#32304=CARTESIAN_POINT('Ctrl Pts',(69.4192635786836,2.36459109474623,339.3147084309));
#32305=CARTESIAN_POINT('Ctrl Pts',(69.4115116051606,2.48300068064472,339.245455297423));
#32306=CARTESIAN_POINT('Ctrl Pts',(69.403762914603,2.60136012001328,339.17623149269));
#32307=CARTESIAN_POINT('Ctrl Pts',(69.3960142240453,2.71688348617671,339.102018650488));
#32308=CARTESIAN_POINT('Ctrl Pts',(69.3882655334877,2.82912969319749,339.023084418897));
#32309=CARTESIAN_POINT('Ctrl Pts',(69.3805184551099,2.94135254645741,338.944166610232));
#32310=CARTESIAN_POINT('Ctrl Pts',(69.372771376732,3.05029927727239,338.860529590793));
#32311=CARTESIAN_POINT('Ctrl Pts',(69.3650242983542,3.15555784351558,338.772484295359));
#32312=CARTESIAN_POINT('Ctrl Pts',(69.3572771550484,3.26081729192708,338.68443826202));
#32313=CARTESIAN_POINT('Ctrl Pts',(69.3495300117426,3.36238821429832,338.591984129781));
#32314=CARTESIAN_POINT('Ctrl Pts',(69.3417828684368,3.4598920348416,338.495472810614));
#32315=CARTESIAN_POINT('Ctrl Pts',(69.3340339834087,3.55741777631341,338.398939793654));
#32316=CARTESIAN_POINT('Ctrl Pts',(69.3262850983806,3.65087431871563,338.298348049624));
#32317=CARTESIAN_POINT('Ctrl Pts',(69.3185362133525,3.73992058907056,338.19408469674));
#32318=CARTESIAN_POINT('Ctrl Pts',(69.3107791035777,3.82906137405711,338.089710677654));
#32319=CARTESIAN_POINT('Ctrl Pts',(69.303021993803,3.91378228179486,337.98165756262));
#32320=CARTESIAN_POINT('Ctrl Pts',(69.2952648840283,3.99378279929591,337.870345277932));
#32321=CARTESIAN_POINT('Ctrl Pts',(69.2875036291021,4.07382606651549,337.758973511518));
#32322=CARTESIAN_POINT('Ctrl Pts',(69.279742374176,4.14914370281404,337.644339431671));
#32323=CARTESIAN_POINT('Ctrl Pts',(69.2719811192498,4.21947962751796,337.526890329132));
#32324=CARTESIAN_POINT('Ctrl Pts',(69.2642074488451,4.28992806677902,337.409253346306));
#32325=CARTESIAN_POINT('Ctrl Pts',(69.2564337784405,4.35537868308554,337.288792685855));
#32326=CARTESIAN_POINT('Ctrl Pts',(69.2486601080358,4.41562189164699,337.165979310268));
#32327=CARTESIAN_POINT('Ctrl Pts',(69.2412483038588,4.47306076435524,337.048882926863));
#32328=CARTESIAN_POINT('Ctrl Pts',(69.2338364996819,4.52576601228643,336.929648200018));
#32329=CARTESIAN_POINT('Ctrl Pts',(69.2264246955049,4.57359798583643,336.808696913928));
#32330=CARTESIAN_POINT('Ctrl Pts',(69.2186496167265,4.62377434689503,336.681817445009));
#32331=CARTESIAN_POINT('Ctrl Pts',(69.210874537948,4.66874621391566,336.552647932275));
#32332=CARTESIAN_POINT('Ctrl Pts',(69.2030994591696,4.70829925112364,336.42165439695));
#32333=CARTESIAN_POINT('Ctrl Pts',(69.1953339481206,4.74780361580127,336.290822057511));
#32334=CARTESIAN_POINT('Ctrl Pts',(69.1875684370716,4.78190230659738,336.158170532155));
#32335=CARTESIAN_POINT('Ctrl Pts',(69.1798029260226,4.81042886515467,336.024186113842));
#32336=CARTESIAN_POINT('Ctrl Pts',(69.1720451145004,4.83892713954608,335.89033454147));
#32337=CARTESIAN_POINT('Ctrl Pts',(69.1642873029782,4.86186419546177,335.755153085976));
#32338=CARTESIAN_POINT('Ctrl Pts',(69.156529491456,4.87912336351415,335.619143170931));
#32339=CARTESIAN_POINT('Ctrl Pts',(69.1487775179329,4.89636954349531,335.483235607659));
#32340=CARTESIAN_POINT('Ctrl Pts',(69.1410255444099,4.90794629138625,335.34650121197));
#32341=CARTESIAN_POINT('Ctrl Pts',(69.1332735708869,4.91378807526547,335.209451220762));
#32342=CARTESIAN_POINT('Ctrl Pts',(69.1255248803293,4.91962738514574,335.072459270307));
#32343=CARTESIAN_POINT('Ctrl Pts',(69.1177761897716,4.91973654503682,334.93515237987));
#32344=CARTESIAN_POINT('Ctrl Pts',(69.110027499214,4.91410192900904,334.798046307759));
#32345=CARTESIAN_POINT('Ctrl Pts',(69.1022804208362,4.9084684853102,334.660968761712));
#32346=CARTESIAN_POINT('Ctrl Pts',(69.0945333424584,4.89709365875272,334.524092341184));
#32347=CARTESIAN_POINT('Ctrl Pts',(69.0867862640806,4.88001594138767,334.38793180584));
#32348=CARTESIAN_POINT('Ctrl Pts',(69.0790391207748,4.86293808089493,334.25177012934));
#32349=CARTESIAN_POINT('Ctrl Pts',(69.071291977469,4.84015728290615,334.116324737826));
#32350=CARTESIAN_POINT('Ctrl Pts',(69.0635448341632,4.81176376770433,333.982103882359));
#32351=CARTESIAN_POINT('Ctrl Pts',(69.0557959491351,4.78336386903753,333.847852851195));
#32352=CARTESIAN_POINT('Ctrl Pts',(69.048047064107,4.74934882308201,333.714827286234));
#32353=CARTESIAN_POINT('Ctrl Pts',(69.040298179079,4.70985959164327,333.583523494898));
#32354=CARTESIAN_POINT('Ctrl Pts',(69.0325410693042,4.67032844592617,333.452080336361));
#32355=CARTESIAN_POINT('Ctrl Pts',(69.0247839595295,4.62531162074379,333.322362976972));
#32356=CARTESIAN_POINT('Ctrl Pts',(69.0170268497548,4.57499961625492,333.194851370727));
#32357=CARTESIAN_POINT('Ctrl Pts',(69.0092655948286,4.52466072663955,333.067271626356));
#32358=CARTESIAN_POINT('Ctrl Pts',(69.0015043399025,4.46902117801145,332.941900340854));
#32359=CARTESIAN_POINT('Ctrl Pts',(68.9937430849763,4.40831852675184,332.819194912608));
#32360=CARTESIAN_POINT('Ctrl Pts',(68.9859694145717,4.34751877103316,332.696293195665));
#32361=CARTESIAN_POINT('Ctrl Pts',(68.978195744167,4.2816399157845,332.576066200685));
#32362=CARTESIAN_POINT('Ctrl Pts',(68.9704220737623,4.21096458505192,332.458945036813));
#32363=CARTESIAN_POINT('Ctrl Pts',(68.9630102695851,4.1435792079672,332.347275891294));
#32364=CARTESIAN_POINT('Ctrl Pts',(68.9555984654079,4.07183401628188,332.238430171505));
#32365=CARTESIAN_POINT('Ctrl Pts',(68.9481866612307,3.99600812490951,332.132753563407));
#32366=CARTESIAN_POINT('Ctrl Pts',(68.9404115824522,3.91646578072868,332.021897429953));
#32367=CARTESIAN_POINT('Ctrl Pts',(68.9326365036738,3.83218123948952,331.914178592456));
#32368=CARTESIAN_POINT('Ctrl Pts',(68.9248614248954,3.74343039899669,331.81002948127));
#32369=CARTESIAN_POINT('Ctrl Pts',(68.9170959138464,3.6547887720633,331.706008532195));
#32370=CARTESIAN_POINT('Ctrl Pts',(68.9093304027974,3.56169203256781,331.605548863728));
#32371=CARTESIAN_POINT('Ctrl Pts',(68.9015648917484,3.46445903446503,331.509053615277));
#32372=CARTESIAN_POINT('Ctrl Pts',(68.8938070802262,3.36732244316268,331.412654042144));
#32373=CARTESIAN_POINT('Ctrl Pts',(68.8860492687039,3.26605803035187,331.320211340206));
#32374=CARTESIAN_POINT('Ctrl Pts',(68.8782914571817,3.16102431730964,331.232094968304));
#32375=CARTESIAN_POINT('Ctrl Pts',(68.8705394836587,3.05606964546772,331.144044906767));
#32376=CARTESIAN_POINT('Ctrl Pts',(68.8627875101358,2.94735161759048,331.060314945162));
#32377=CARTESIAN_POINT('Ctrl Pts',(68.8550355366128,2.83526468060926,330.9812368503));
#32378=CARTESIAN_POINT('Ctrl Pts',(68.8472868460552,2.7232252125121,330.902192245057));
#32379=CARTESIAN_POINT('Ctrl Pts',(68.8395381554975,2.60781999170988,330.827795813093));
#32380=CARTESIAN_POINT('Ctrl Pts',(68.8317894649399,2.48947535659532,330.758338119156));
#32381=CARTESIAN_POINT('Ctrl Pts',(68.8240423865621,2.37115534407044,330.688894876473));
#32382=CARTESIAN_POINT('Ctrl Pts',(68.8162953081842,2.2498974705799,330.624388525681));
#32383=CARTESIAN_POINT('Ctrl Pts',(68.8085482298064,2.12615543876557,330.565065263986));
#32384=CARTESIAN_POINT('Ctrl Pts',(68.8008010865006,2.00241236987407,330.505741505104));
#32385=CARTESIAN_POINT('Ctrl Pts',(68.7930539431948,1.87618545359561,330.451601090937));
#32386=CARTESIAN_POINT('Ctrl Pts',(68.785306799889,1.74795091246184,330.402843197135));
#32387=CARTESIAN_POINT('Ctrl Pts',(68.7775579148609,1.61968754148019,330.354074341524));
#32388=CARTESIAN_POINT('Ctrl Pts',(68.7698090298327,1.48941601277807,330.310690553141));
#32389=CARTESIAN_POINT('Ctrl Pts',(68.7620601448046,1.35762996437586,330.272841874622));
#32390=CARTESIAN_POINT('Ctrl Pts',(68.7543030350299,1.22570403690073,330.234953023124));
#32391=CARTESIAN_POINT('Ctrl Pts',(68.7465459252551,1.0922607548206,330.202611125466));
#32392=CARTESIAN_POINT('Ctrl Pts',(68.7387888154804,0.957806812257021,330.175915716647));
#32393=CARTESIAN_POINT('Ctrl Pts',(68.7310275605542,0.823281021805727,330.149206042655));
#32394=CARTESIAN_POINT('Ctrl Pts',(68.7232663056281,0.687743880788366,330.128148929726));
#32395=CARTESIAN_POINT('Ctrl Pts',(68.7155050507019,0.551708580656278,330.112792136145));
#32396=CARTESIAN_POINT('Ctrl Pts',(68.7077313802973,0.415455668377595,330.097410776698));
#32397=CARTESIAN_POINT('Ctrl Pts',(68.6999577098926,0.278703394664759,330.087747985933));
#32398=CARTESIAN_POINT('Ctrl Pts',(68.6921840394879,0.141967232484869,330.083799397156));
#32399=CARTESIAN_POINT('Ctrl Pts',(68.6847722353109,0.0115961715527522,
330.080034616137));
#32400=CARTESIAN_POINT('Ctrl Pts',(68.6773604311339,-0.118759956294964,
330.081464013898));
#32401=CARTESIAN_POINT('Ctrl Pts',(68.6699486269569,-0.248659411263507,
330.088039947262));
#32402=CARTESIAN_POINT('Ctrl Pts',(68.6621735481784,-0.384925625472301,
330.09493818671));
#32403=CARTESIAN_POINT('Ctrl Pts',(68.6543984694,-0.521119895514062,330.107522011695));
#32404=CARTESIAN_POINT('Ctrl Pts',(68.6466233906216,-0.656729277347898,
330.125793426744));
#32405=CARTESIAN_POINT('Ctrl Pts',(68.6388578795725,-0.792171783203887,
330.144042357653));
#32406=CARTESIAN_POINT('Ctrl Pts',(68.6310923685235,-0.927030449261685,
330.167964901045));
#32407=CARTESIAN_POINT('Ctrl Pts',(68.6233268574745,-1.06079371682242,330.197511087691));
#32408=CARTESIAN_POINT('Ctrl Pts',(68.6155690459523,-1.19442435771365,330.227027979207));
#32409=CARTESIAN_POINT('Ctrl Pts',(68.6078112344301,-1.3269613822743,330.262157333941));
#32410=CARTESIAN_POINT('Ctrl Pts',(68.6000534229079,-1.45790008824687,330.302797599082));
#32411=CARTESIAN_POINT('Ctrl Pts',(68.5923014493849,-1.58874025869097,330.343407281134));
#32412=CARTESIAN_POINT('Ctrl Pts',(68.5845494758619,-1.71798413282898,330.389519503525));
#32413=CARTESIAN_POINT('Ctrl Pts',(68.5767975023389,-1.84513926300358,330.440982105472));
#32414=CARTESIAN_POINT('Ctrl Pts',(68.5690488117812,-1.97224054290524,330.492422912977));
#32415=CARTESIAN_POINT('Ctrl Pts',(68.5613001212236,-2.09725447664881,330.54920944701));
#32416=CARTESIAN_POINT('Ctrl Pts',(68.553551430666,-2.21970600596944,330.611140431779));
#32417=CARTESIAN_POINT('Ctrl Pts',(68.5458043522882,-2.34213205822649,330.67305853129));
#32418=CARTESIAN_POINT('Ctrl Pts',(68.5380572739103,-2.46199641791078,330.740118776244));
#32419=CARTESIAN_POINT('Ctrl Pts',(68.5303101955325,-2.57884652800746,330.812072869846));
#32420=CARTESIAN_POINT('Ctrl Pts',(68.5225630522267,-2.69569761742069,330.884027566492));
#32421=CARTESIAN_POINT('Ctrl Pts',(68.5148159089209,-2.80953407402629,330.960875988641));
#32422=CARTESIAN_POINT('Ctrl Pts',(68.507068765615,-2.91993069543224,331.042325455981));
#32423=CARTESIAN_POINT('Ctrl Pts',(68.4993198805869,-3.03035213634224,331.123793234891));
#32424=CARTESIAN_POINT('Ctrl Pts',(68.4915709955589,-3.13733188870471,331.209863885342));
#32425=CARTESIAN_POINT('Ctrl Pts',(68.4838221105308,-3.2404766426096,331.300203493271));
#32426=CARTESIAN_POINT('Ctrl Pts',(68.4760650007561,-3.3437308754219,331.390638988594));
#32427=CARTESIAN_POINT('Ctrl Pts',(68.4683078909813,-3.44314168405402,331.485352234782));
#32428=CARTESIAN_POINT('Ctrl Pts',(68.4605507812066,-3.53835116613823,331.583971006038));
#32429=CARTESIAN_POINT('Ctrl Pts',(68.4527895262805,-3.63361152512546,331.682642476012));
#32430=CARTESIAN_POINT('Ctrl Pts',(68.4450282713543,-3.72466582474512,331.785223337389));
#32431=CARTESIAN_POINT('Ctrl Pts',(68.4372670164281,-3.81119618669597,331.891307881276));
#32432=CARTESIAN_POINT('Ctrl Pts',(68.4294933460235,-3.89786496902588,331.997562125861));
#32433=CARTESIAN_POINT('Ctrl Pts',(68.4217196756188,-3.97999511807655,332.107330939774));
#32434=CARTESIAN_POINT('Ctrl Pts',(68.4139460052141,-4.05731135389337,332.220178487732));
#32435=CARTESIAN_POINT('Ctrl Pts',(68.406534201037,-4.13102850033182,332.327772955183));
#32436=CARTESIAN_POINT('Ctrl Pts',(68.3991223968599,-4.20036966987215,332.438165733265));
#32437=CARTESIAN_POINT('Ctrl Pts',(68.3917105926828,-4.26513587592794,332.550959571103));
#32438=CARTESIAN_POINT('Ctrl Pts',(68.3836106157741,-4.33591550811773,332.674226114593));
#32439=CARTESIAN_POINT('Ctrl Pts',(68.3755106388654,-4.401439174065,332.800722637179));
#32440=CARTESIAN_POINT('Ctrl Pts',(68.3674106619567,-4.46141296734486,332.929981305083));
#32441=CARTESIAN_POINT('Ctrl Pts',(68.359323648681,-4.52129077538237,333.059033100552));
#32442=CARTESIAN_POINT('Ctrl Pts',(68.3512366354052,-4.57563626180767,333.19083792405));
#32443=CARTESIAN_POINT('Ctrl Pts',(68.3431496221295,-4.62420032361822,333.324901665708));
#32444=CARTESIAN_POINT('Ctrl Pts',(68.3350791102444,-4.67266529142197,333.458691852955));
#32445=CARTESIAN_POINT('Ctrl Pts',(68.3270085983591,-4.71537223973322,333.594731445541));
#32446=CARTESIAN_POINT('Ctrl Pts',(68.3189380864739,-4.75211955942271,333.732505323304));
#32447=CARTESIAN_POINT('Ctrl Pts',(68.3108772009443,-4.78882304759698,333.870114866965));
#32448=CARTESIAN_POINT('Ctrl Pts',(68.3028163154146,-4.81958097740674,334.009454244478));
#32449=CARTESIAN_POINT('Ctrl Pts',(68.294755429885,-4.84424064846224,334.149990822234));
#32450=CARTESIAN_POINT('Ctrl Pts',(68.2867065378168,-4.86886362940282,334.290318301371));
#32451=CARTESIAN_POINT('Ctrl Pts',(68.2786576457488,-4.88740638320064,334.431839091039));
#32452=CARTESIAN_POINT('Ctrl Pts',(68.2706087536806,-4.89976675740206,334.574008467739));
#32453=CARTESIAN_POINT('Ctrl Pts',(68.2625845852838,-4.91208916441178,334.715741144718));
#32454=CARTESIAN_POINT('Ctrl Pts',(68.2545604168869,-4.91826706186341,334.858118091645));
#32455=CARTESIAN_POINT('Ctrl Pts',(68.24653624849,-4.91824996458602,335.000590211503));
#32456=CARTESIAN_POINT('',(71.7465372896154,-4.92216623067323,335.00168803465));
#32457=CARTESIAN_POINT('Ctrl Pts',(71.7465362484899,-4.91824970447095,335.001704984294));
#32458=CARTESIAN_POINT('Ctrl Pts',(71.7412131669834,-4.91821730456371,335.095166745058));
#32459=CARTESIAN_POINT('Ctrl Pts',(71.7358900854768,-4.91552100689044,335.18857910669));
#32460=CARTESIAN_POINT('Ctrl Pts',(71.7305670039701,-4.9101680900388,335.281837524231));
#32461=CARTESIAN_POINT('Ctrl Pts',(71.7227919251917,-4.9023494327133,335.418054026315));
#32462=CARTESIAN_POINT('Ctrl Pts',(71.7150168464133,-4.88884580562974,335.554160175694));
#32463=CARTESIAN_POINT('Ctrl Pts',(71.7072417676348,-4.86965866961016,335.689643026493));
#32464=CARTESIAN_POINT('Ctrl Pts',(71.6994762565858,-4.85049514458297,335.824959157019));
#32465=CARTESIAN_POINT('Ctrl Pts',(71.6917107455368,-4.82566208079924,335.959653131777));
#32466=CARTESIAN_POINT('Ctrl Pts',(71.6839452344878,-4.79521290228959,336.093213741322));
#32467=CARTESIAN_POINT('Ctrl Pts',(71.6761874229656,-4.76479391422907,336.226641925134));
#32468=CARTESIAN_POINT('Ctrl Pts',(71.6684296114434,-4.72876997918441,336.358938601386));
#32469=CARTESIAN_POINT('Ctrl Pts',(71.6606717999212,-4.68724605727273,336.4895997654));
#32470=CARTESIAN_POINT('Ctrl Pts',(71.6529198263981,-4.64575338342915,336.620162602745));
#32471=CARTESIAN_POINT('Ctrl Pts',(71.6451678528751,-4.59876907893377,336.749092006634));
#32472=CARTESIAN_POINT('Ctrl Pts',(71.6374158793521,-4.54644862793027,336.875896568602));
#32473=CARTESIAN_POINT('Ctrl Pts',(71.6296671887945,-4.49415033466883,337.002647428762));
#32474=CARTESIAN_POINT('Ctrl Pts',(71.6219184982369,-4.43652053837923,337.127274876208));
#32475=CARTESIAN_POINT('Ctrl Pts',(71.6141698076792,-4.37376371961623,337.249305223279));
#32476=CARTESIAN_POINT('Ctrl Pts',(71.6064227293014,-4.31101995793353,337.371310180916));
#32477=CARTESIAN_POINT('Ctrl Pts',(71.5986756509236,-4.2431514742083,337.490718765585));
#32478=CARTESIAN_POINT('Ctrl Pts',(71.5909285725458,-4.17040961691579,337.607080108021));
#32479=CARTESIAN_POINT('Ctrl Pts',(71.58318142924,-4.09766714997654,337.723442425676));
#32480=CARTESIAN_POINT('Ctrl Pts',(71.5754342859342,-4.02005143520023,337.836757118717));
#32481=CARTESIAN_POINT('Ctrl Pts',(71.5676871426284,-3.9378580187657,337.94660097172));
#32482=CARTESIAN_POINT('Ctrl Pts',(71.5599382576003,-3.85564612350614,338.056469519954));
#32483=CARTESIAN_POINT('Ctrl Pts',(71.5521893725722,-3.76885471279912,338.162865362505));
#32484=CARTESIAN_POINT('Ctrl Pts',(71.5444404875441,-3.67782035017689,338.265397454266));
#32485=CARTESIAN_POINT('Ctrl Pts',(71.5366833777694,-3.58668936274155,338.368038374648));
#32486=CARTESIAN_POINT('Ctrl Pts',(71.5289262679946,-3.49130668712623,338.466807059305));
#32487=CARTESIAN_POINT('Ctrl Pts',(71.5211691582199,-3.3920469585192,338.561348128687));
#32488=CARTESIAN_POINT('Ctrl Pts',(71.5134079032938,-3.29273418868691,338.655939717793));
#32489=CARTESIAN_POINT('Ctrl Pts',(71.5056466483676,-3.18954053159051,338.746298932791));
#32490=CARTESIAN_POINT('Ctrl Pts',(71.4978853934414,-3.08287383435791,338.832110643488));
#32491=CARTESIAN_POINT('Ctrl Pts',(71.4901117230368,-2.97603650517234,338.918059624955));
#32492=CARTESIAN_POINT('Ctrl Pts',(71.4823380526321,-2.86571534856039,338.999446333297));
#32493=CARTESIAN_POINT('Ctrl Pts',(71.4745643822274,-2.75234804957195,339.075998439219));
#32494=CARTESIAN_POINT('Ctrl Pts',(71.4671525780504,-2.64425802562663,339.148987026193));
#32495=CARTESIAN_POINT('Ctrl Pts',(71.4597407738734,-2.53339931774793,339.217580831547));
#32496=CARTESIAN_POINT('Ctrl Pts',(71.4523289696963,-2.42017051204073,339.28158355695));
#32497=CARTESIAN_POINT('Ctrl Pts',(71.4445538909179,-2.30139202527402,339.34872324658));
#32498=CARTESIAN_POINT('Ctrl Pts',(71.4367788121394,-2.17962987311048,339.411022605677));
#32499=CARTESIAN_POINT('Ctrl Pts',(71.429003733361,-2.05531619321631,339.46820527823));
#32500=CARTESIAN_POINT('Ctrl Pts',(71.421238222312,-1.93115548921944,339.525317583864));
#32501=CARTESIAN_POINT('Ctrl Pts',(71.413472711263,-1.80444985654074,339.577325569219));
#32502=CARTESIAN_POINT('Ctrl Pts',(71.405707200214,-1.67565809291909,339.623997514936));
#32503=CARTESIAN_POINT('Ctrl Pts',(71.3979493886918,-1.54699402670612,339.670623185283));
#32504=CARTESIAN_POINT('Ctrl Pts',(71.3901915771696,-1.41624831091442,339.711923212469));
#32505=CARTESIAN_POINT('Ctrl Pts',(71.3824337656474,-1.28390157377272,339.747713113844));
#32506=CARTESIAN_POINT('Ctrl Pts',(71.3746817921244,-1.15165443174776,339.783476082183));
#32507=CARTESIAN_POINT('Ctrl Pts',(71.3669298186014,-1.0178090423085,339.813737076578));
#32508=CARTESIAN_POINT('Ctrl Pts',(71.3591778450784,-0.882862782708903,
339.838360917646));
#32509=CARTESIAN_POINT('Ctrl Pts',(71.3514291545208,-0.747973672930176,
339.862974330503));
#32510=CARTESIAN_POINT('Ctrl Pts',(71.3436804639632,-0.611985003993076,
339.88195526826));
#32511=CARTESIAN_POINT('Ctrl Pts',(71.3359317734056,-0.475405766120146,
339.895219343404));
#32512=CARTESIAN_POINT('Ctrl Pts',(71.3281846950277,-0.338854944698388,
339.908480658847));
#32513=CARTESIAN_POINT('Ctrl Pts',(71.3204376166499,-0.201714187543178,
339.916027439799));
#32514=CARTESIAN_POINT('Ctrl Pts',(71.3126905382721,-0.0644986593213518,
339.917827059327));
#32515=CARTESIAN_POINT('Ctrl Pts',(71.3049433949663,0.0727180188987628,
339.919626693937));
#32516=CARTESIAN_POINT('Ctrl Pts',(71.2971962516605,0.210009078594723,339.915679065923));
#32517=CARTESIAN_POINT('Ctrl Pts',(71.2894491083546,0.346858691890955,339.906003680223));
#32518=CARTESIAN_POINT('Ctrl Pts',(71.2817002233266,0.483739071885563,339.89632611929));
#32519=CARTESIAN_POINT('Ctrl Pts',(71.2739513382984,0.620177418166119,339.88091826581));
#32520=CARTESIAN_POINT('Ctrl Pts',(71.2662024532703,0.755662758719872,339.85985152629));
#32521=CARTESIAN_POINT('Ctrl Pts',(71.2584453434956,0.891291904813915,339.838762426315));
#32522=CARTESIAN_POINT('Ctrl Pts',(71.2506882337209,1.02596563771167,339.812002502104));
#32523=CARTESIAN_POINT('Ctrl Pts',(71.2429311239462,1.15918237457085,339.779694476113));
#32524=CARTESIAN_POINT('Ctrl Pts',(71.23516986902,1.29247029819477,339.747369185745));
#32525=CARTESIAN_POINT('Ctrl Pts',(71.2274086140938,1.42429929892198,339.709489994));
#32526=CARTESIAN_POINT('Ctrl Pts',(71.2196473591676,1.55418366756549,339.666229333195));
#32527=CARTESIAN_POINT('Ctrl Pts',(71.211873688763,1.68427580886961,339.622899469433));
#32528=CARTESIAN_POINT('Ctrl Pts',(71.2041000183583,1.81241673629315,339.574171073091));
#32529=CARTESIAN_POINT('Ctrl Pts',(71.1963263479537,1.93814058582717,339.52026482986));
#32530=CARTESIAN_POINT('Ctrl Pts',(71.1889145437766,2.05801195991865,339.46886793522));
#32531=CARTESIAN_POINT('Ctrl Pts',(71.1815027395994,2.17568596213188,339.412764526687));
#32532=CARTESIAN_POINT('Ctrl Pts',(71.1740909354223,2.29078182319854,339.352183555527));
#32533=CARTESIAN_POINT('Ctrl Pts',(71.1663158566439,2.41151887526843,339.288633330511));
#32534=CARTESIAN_POINT('Ctrl Pts',(71.1585407778654,2.5298002226781,339.219954697018));
#32535=CARTESIAN_POINT('Ctrl Pts',(71.150765699087,2.64515961727508,339.146361496739));
#32536=CARTESIAN_POINT('Ctrl Pts',(71.143000188038,2.7603770547928,339.072858857577));
#32537=CARTESIAN_POINT('Ctrl Pts',(71.135234676989,2.87267936742943,338.994453893005));
#32538=CARTESIAN_POINT('Ctrl Pts',(71.12746916594,2.98162341565095,338.911407019187));
#32539=CARTESIAN_POINT('Ctrl Pts',(71.1197113544178,3.0904594455314,338.828442486586));
#32540=CARTESIAN_POINT('Ctrl Pts',(71.1119535428956,3.19594352849189,338.740845439344));
#32541=CARTESIAN_POINT('Ctrl Pts',(71.1041957313734,3.29766043362354,338.648920213846));
#32542=CARTESIAN_POINT('Ctrl Pts',(71.0964437578504,3.39930079355852,338.557064164995));
#32543=CARTESIAN_POINT('Ctrl Pts',(71.0886917843274,3.4971793296083,338.460886681992));
#32544=CARTESIAN_POINT('Ctrl Pts',(71.0809398108044,3.59091320717331,338.36073286666));
#32545=CARTESIAN_POINT('Ctrl Pts',(71.0731911202468,3.68460738838553,338.260621466528));
#32546=CARTESIAN_POINT('Ctrl Pts',(71.0654424296892,3.77416013567615,338.156537368174));
#32547=CARTESIAN_POINT('Ctrl Pts',(71.0576937391316,3.85922504196941,338.048862925409));
#32548=CARTESIAN_POINT('Ctrl Pts',(71.0499466607537,3.94427224979843,337.941210885212));
#32549=CARTESIAN_POINT('Ctrl Pts',(71.0421995823759,4.02483323173668,337.829970292958));
#32550=CARTESIAN_POINT('Ctrl Pts',(71.0344525039981,4.10060176593665,337.7155567053));
#32551=CARTESIAN_POINT('Ctrl Pts',(71.0267053606923,4.17637093514987,337.601142158745));
#32552=CARTESIAN_POINT('Ctrl Pts',(71.0189582173865,4.2473473606952,337.483554889638));
#32553=CARTESIAN_POINT('Ctrl Pts',(71.0112110740806,4.31326830062813,337.363239223882));
#32554=CARTESIAN_POINT('Ctrl Pts',(71.0034621890526,4.37920406098791,337.242896508611));
#32555=CARTESIAN_POINT('Ctrl Pts',(70.9957133040245,4.44008188628708,337.119824518819));
#32556=CARTESIAN_POINT('Ctrl Pts',(70.9879644189964,4.49568530750658,336.99449158393));
#32557=CARTESIAN_POINT('Ctrl Pts',(70.9802073092217,4.55134774677189,336.86902561937));
#32558=CARTESIAN_POINT('Ctrl Pts',(70.9724501994469,4.60172444005301,336.741294273764));
#32559=CARTESIAN_POINT('Ctrl Pts',(70.9646930896722,4.64664715202462,336.611785750986));
#32560=CARTESIAN_POINT('Ctrl Pts',(70.956931834746,4.69159386925713,336.482208022995));
#32561=CARTESIAN_POINT('Ctrl Pts',(70.9491705798199,4.73108068544076,336.350851599674));
#32562=CARTESIAN_POINT('Ctrl Pts',(70.9414093248937,4.76498975748128,336.218218237262));
#32563=CARTESIAN_POINT('Ctrl Pts',(70.9336356544891,4.79895307298612,336.085372704696));
#32564=CARTESIAN_POINT('Ctrl Pts',(70.9258619840844,4.82732073348177,335.951246533764));
#32565=CARTESIAN_POINT('Ctrl Pts',(70.9180883136798,4.85002621252508,335.816350905138));
#32566=CARTESIAN_POINT('Ctrl Pts',(70.9106765095027,4.8716747460562,335.687734700479));
#32567=CARTESIAN_POINT('Ctrl Pts',(70.9032647053256,4.88817634763701,335.558419347984));
#32568=CARTESIAN_POINT('Ctrl Pts',(70.8958529011486,4.89951749117312,335.428848943322));
#32569=CARTESIAN_POINT('Ctrl Pts',(70.8880778223701,4.91141449793752,335.292927907157));
#32570=CARTESIAN_POINT('Ctrl Pts',(70.8803027435917,4.91766999390518,335.156296649336));
#32571=CARTESIAN_POINT('Ctrl Pts',(70.8725276648133,4.91821148948509,335.019462969887));
#32572=CARTESIAN_POINT('Ctrl Pts',(70.8647621537643,4.91875231872022,334.882797672991));
#32573=CARTESIAN_POINT('Ctrl Pts',(70.8569966427153,4.91359313658753,334.745930837224));
#32574=CARTESIAN_POINT('Ctrl Pts',(70.8492311316662,4.90271312436751,334.609376034203));
#32575=CARTESIAN_POINT('Ctrl Pts',(70.841473320144,4.89184389971127,334.472956625668));
#32576=CARTESIAN_POINT('Ctrl Pts',(70.8337155086218,4.87526516385015,334.336849021322));
#32577=CARTESIAN_POINT('Ctrl Pts',(70.8259576970996,4.85300813447139,334.201567091576));
#32578=CARTESIAN_POINT('Ctrl Pts',(70.8182057235766,4.83076785421308,334.066386965772));
#32579=CARTESIAN_POINT('Ctrl Pts',(70.8104537500536,4.80285784902508,333.932031661945));
#32580=CARTESIAN_POINT('Ctrl Pts',(70.8027017765306,4.76936114862362,333.799009868276));
#32581=CARTESIAN_POINT('Ctrl Pts',(70.7949530859729,4.73587863409464,333.666044409414));
#32582=CARTESIAN_POINT('Ctrl Pts',(70.7872043954153,4.69681422534648,333.53441171573));
#32583=CARTESIAN_POINT('Ctrl Pts',(70.7794557048577,4.65230199111062,333.404610001909));
#32584=CARTESIAN_POINT('Ctrl Pts',(70.7717086264798,4.60779901801685,333.274835294419));
#32585=CARTESIAN_POINT('Ctrl Pts',(70.763961548102,4.55785060069146,333.146891178562));
#32586=CARTESIAN_POINT('Ctrl Pts',(70.7562144697241,4.50264047537589,333.02126004437));
#32587=CARTESIAN_POINT('Ctrl Pts',(70.7484673264183,4.44742988734638,332.895627857268));
#32588=CARTESIAN_POINT('Ctrl Pts',(70.7407201831125,4.38695766062848,332.772309048342));
#32589=CARTESIAN_POINT('Ctrl Pts',(70.7329730398067,4.32145525361317,332.651765013139));
#32590=CARTESIAN_POINT('Ctrl Pts',(70.7252241547786,4.25593812026611,332.531193877078));
#32591=CARTESIAN_POINT('Ctrl Pts',(70.7174752697505,4.18538874286202,332.413399099466));
#32592=CARTESIAN_POINT('Ctrl Pts',(70.7097263847224,4.11008380579922,332.298816153645));
#32593=CARTESIAN_POINT('Ctrl Pts',(70.7019692749477,4.03469893929813,332.184111588302));
#32594=CARTESIAN_POINT('Ctrl Pts',(70.694212165173,3.95454864509715,332.072625991852));
#32595=CARTESIAN_POINT('Ctrl Pts',(70.6864550553982,3.86995242246284,331.964765032098));
#32596=CARTESIAN_POINT('Ctrl Pts',(70.678693800472,3.78531099431202,331.856846434897));
#32597=CARTESIAN_POINT('Ctrl Pts',(70.6709325455458,3.69621915756468,331.752556630864));
#32598=CARTESIAN_POINT('Ctrl Pts',(70.6631712906197,3.60303507808759,331.652266245866));
#32599=CARTESIAN_POINT('Ctrl Pts',(70.655397620215,3.50970193445195,331.551815428936));
#32600=CARTESIAN_POINT('Ctrl Pts',(70.6476239498103,3.4122637446887,331.455377090778));
#32601=CARTESIAN_POINT('Ctrl Pts',(70.6398502794056,3.31111437025545,331.363283804091));
#32602=CARTESIAN_POINT('Ctrl Pts',(70.6324384752286,3.21467352353712,331.275477482056));
#32603=CARTESIAN_POINT('Ctrl Pts',(70.6250266710515,3.11485944827854,331.191620975891));
#32604=CARTESIAN_POINT('Ctrl Pts',(70.6176148668744,3.01203827425644,331.111965985628));
#32605=CARTESIAN_POINT('Ctrl Pts',(70.6098397880959,2.90417752820712,331.028406867012));
#32606=CARTESIAN_POINT('Ctrl Pts',(70.6020647093175,2.79266659641416,330.949207473491));
#32607=CARTESIAN_POINT('Ctrl Pts',(70.5942896305391,2.67789327047571,330.874703562841));
#32608=CARTESIAN_POINT('Ctrl Pts',(70.58652411949,2.56326118042166,330.800291333995));
#32609=CARTESIAN_POINT('Ctrl Pts',(70.578758608441,2.44537500881328,330.730563302066));
#32610=CARTESIAN_POINT('Ctrl Pts',(70.570993097392,2.32465536277718,330.66581489703));
#32611=CARTESIAN_POINT('Ctrl Pts',(70.5632352858698,2.20405541062159,330.601130690225));
#32612=CARTESIAN_POINT('Ctrl Pts',(70.5554774743476,2.08062791713669,330.541416468338));
#32613=CARTESIAN_POINT('Ctrl Pts',(70.5477196628254,1.95482190059504,330.486924064515));
#32614=CARTESIAN_POINT('Ctrl Pts',(70.5399676893024,1.82911055707046,330.432472667954));
#32615=CARTESIAN_POINT('Ctrl Pts',(70.5322157157794,1.70102461045468,330.383235422544));
#32616=CARTESIAN_POINT('Ctrl Pts',(70.5244637422564,1.57103675963464,330.339417787188));
#32617=CARTESIAN_POINT('Ctrl Pts',(70.5167150516988,1.4411039587466,330.295618708628));
#32618=CARTESIAN_POINT('Ctrl Pts',(70.5089663611411,1.30927122527812,330.257234799712));
#32619=CARTESIAN_POINT('Ctrl Pts',(70.5012176705835,1.1760300708719,330.224422931739));
#32620=CARTESIAN_POINT('Ctrl Pts',(70.4934705922057,1.0428166384007,330.191617890549));
#32621=CARTESIAN_POINT('Ctrl Pts',(70.4857235138278,0.908195747153761,330.164382677758));
#32622=CARTESIAN_POINT('Ctrl Pts',(70.47797643545,0.77267247942467,330.142823834568));
#32623=CARTESIAN_POINT('Ctrl Pts',(70.4702292921442,0.637148075880062,330.121264810694));
#32624=CARTESIAN_POINT('Ctrl Pts',(70.4624821488384,0.500721666789251,330.105382312718));
#32625=CARTESIAN_POINT('Ctrl Pts',(70.4547350055326,0.363906504929608,330.095231389946));
#32626=CARTESIAN_POINT('Ctrl Pts',(70.4469861205045,0.227060584117003,330.085078185031));
#32627=CARTESIAN_POINT('Ctrl Pts',(70.4392372354764,0.0898261263462719,
330.080659148367));
#32628=CARTESIAN_POINT('Ctrl Pts',(70.4314883504483,-0.0472809397553424,
330.081977269752));
#32629=CARTESIAN_POINT('Ctrl Pts',(70.4237312406736,-0.184533532713591,
330.083296790205));
#32630=CARTESIAN_POINT('Ctrl Pts',(70.4159741308988,-0.321658072424833,
330.090365629248));
#32631=CARTESIAN_POINT('Ctrl Pts',(70.4082170211241,-0.458140524791754,
330.10313464326));
#32632=CARTESIAN_POINT('Ctrl Pts',(70.4004557661979,-0.594695909017264,
330.115910480624));
#32633=CARTESIAN_POINT('Ctrl Pts',(70.3926945112718,-0.730608135105816,
330.134392509726));
#32634=CARTESIAN_POINT('Ctrl Pts',(70.3849332563456,-0.865371711759068,
330.15848010817));
#32635=CARTESIAN_POINT('Ctrl Pts',(70.3771595859409,-1.00035086621562,330.182606238921));
#32636=CARTESIAN_POINT('Ctrl Pts',(70.3693859155363,-1.13417731767726,330.212355773038));
#32637=CARTESIAN_POINT('Ctrl Pts',(70.3616122451316,-1.26635825763189,330.247577478188));
#32638=CARTESIAN_POINT('Ctrl Pts',(70.3542004409546,-1.39238614302976,330.281159604489));
#32639=CARTESIAN_POINT('Ctrl Pts',(70.3467886367776,-1.51691799151516,330.319715822643));
#32640=CARTESIAN_POINT('Ctrl Pts',(70.3393768326005,-1.63954400933231,330.363074455637));
#32641=CARTESIAN_POINT('Ctrl Pts',(70.3316017538221,-1.76818029356765,330.408558224394));
#32642=CARTESIAN_POINT('Ctrl Pts',(70.3238266750437,-1.89512571691326,330.459470809625));
#32643=CARTESIAN_POINT('Ctrl Pts',(70.3160515962652,-2.01988807720766,330.515667806902));
#32644=CARTESIAN_POINT('Ctrl Pts',(70.3082860852162,-2.14449690947495,330.571795650196));
#32645=CARTESIAN_POINT('Ctrl Pts',(70.3005205741672,-2.26692767087084,330.633194807822));
#32646=CARTESIAN_POINT('Ctrl Pts',(70.2927550631182,-2.38670431337455,330.699671456386));
#32647=CARTESIAN_POINT('Ctrl Pts',(70.284997251596,-2.50636219698866,330.76608219316));
#32648=CARTESIAN_POINT('Ctrl Pts',(70.2772394400738,-2.62337085911305,330.837560213777));
#32649=CARTESIAN_POINT('Ctrl Pts',(70.2694816285516,-2.73727553833108,330.913864210559));
#32650=CARTESIAN_POINT('Ctrl Pts',(70.2617296550286,-2.85109450066557,330.990110786162));
#32651=CARTESIAN_POINT('Ctrl Pts',(70.2539776815056,-2.96181380604507,331.071175892541));
#32652=CARTESIAN_POINT('Ctrl Pts',(70.2462257079826,-3.06900487520345,331.156773212719));
#32653=CARTESIAN_POINT('Ctrl Pts',(70.238477017425,-3.17615054888047,331.24233428238));
#32654=CARTESIAN_POINT('Ctrl Pts',(70.2307283268674,-3.2797706534131,331.332423504899));
#32655=CARTESIAN_POINT('Ctrl Pts',(70.2229796363098,-3.37946728722723,331.426712449709));
#32656=CARTESIAN_POINT('Ctrl Pts',(70.2152325579319,-3.479143178324,331.520981776918));
#32657=CARTESIAN_POINT('Ctrl Pts',(70.2074854795541,-3.5748969385962,331.619448819981));
#32658=CARTESIAN_POINT('Ctrl Pts',(70.1997384011763,-3.66636564626394,331.72174649998));
#32659=CARTESIAN_POINT('Ctrl Pts',(70.1919912578705,-3.75783512052749,331.824045037332));
#32660=CARTESIAN_POINT('Ctrl Pts',(70.1842441145647,-3.8450192100189,331.930173984273));
#32661=CARTESIAN_POINT('Ctrl Pts',(70.1764969712589,-3.92759387207261,332.039731525933));
#32662=CARTESIAN_POINT('Ctrl Pts',(70.1687480862308,-4.01018709866346,332.149313698453));
#32663=CARTESIAN_POINT('Ctrl Pts',(70.1609992012027,-4.08816860048186,332.262325687458));
#32664=CARTESIAN_POINT('Ctrl Pts',(70.1532503161746,-4.16125666475779,332.378335255509));
#32665=CARTESIAN_POINT('Ctrl Pts',(70.1454932063999,-4.23442230546034,332.494467957314));
#32666=CARTESIAN_POINT('Ctrl Pts',(70.1377360966252,-4.30268392454371,332.613604262597));
#32667=CARTESIAN_POINT('Ctrl Pts',(70.1299789868505,-4.36580467458381,332.735285314685));
#32668=CARTESIAN_POINT('Ctrl Pts',(70.1222177319243,-4.42895915433449,332.857031389236));
#32669=CARTESIAN_POINT('Ctrl Pts',(70.1144564769981,-4.48696712594403,332.98132456616));
#32670=CARTESIAN_POINT('Ctrl Pts',(70.106695222072,-4.53963965458598,333.107685314486));
#32671=CARTESIAN_POINT('Ctrl Pts',(70.0989215516673,-4.59239644210783,333.234248198829));
#32672=CARTESIAN_POINT('Ctrl Pts',(70.0911478812627,-4.63980059603682,333.362884896864));
#32673=CARTESIAN_POINT('Ctrl Pts',(70.083374210858,-4.68171260390408,333.493099154906));
#32674=CARTESIAN_POINT('Ctrl Pts',(70.0759624066808,-4.72167359772205,333.61725190791));
#32675=CARTESIAN_POINT('Ctrl Pts',(70.0685506025037,-4.75664218016783,333.742838378072));
#32676=CARTESIAN_POINT('Ctrl Pts',(70.0611387983266,-4.78654095518772,333.869421056799));
#32677=CARTESIAN_POINT('Ctrl Pts',(70.0503717066871,-4.82997475927267,334.053307094428));
#32678=CARTESIAN_POINT('Ctrl Pts',(70.0396046150477,-4.8628271733437,334.239780564964));
#32679=CARTESIAN_POINT('Ctrl Pts',(70.0288375234083,-4.88485179693977,334.427805990564));
#32680=CARTESIAN_POINT('Ctrl Pts',(70.0180704317688,-4.90687642053583,334.615831416164));
#32681=CARTESIAN_POINT('Ctrl Pts',(70.0073033401294,-4.91807308447629,334.805409443769));
#32682=CARTESIAN_POINT('Ctrl Pts',(69.99653624849,-4.91824791922601,334.995475894668));
#32683=CARTESIAN_POINT('',(73.4965351039332,-4.91545634990101,335.003629922274));
#32684=CARTESIAN_POINT('Ctrl Pts',(73.4965341419554,-4.91310945567289,335.003645225589));
#32685=CARTESIAN_POINT('Ctrl Pts',(73.4643544978415,-4.91696488633254,335.573219306921));
#32686=CARTESIAN_POINT('Ctrl Pts',(73.339428842303,-4.56197822582132,337.779717770033));
#32687=CARTESIAN_POINT('Ctrl Pts',(73.12175717534,-1.29865199811852,340.669034472837));
#32688=CARTESIAN_POINT('Ctrl Pts',(72.8435191410659,4.06443691893726,339.159904013125));
#32689=CARTESIAN_POINT('Ctrl Pts',(72.5652811067921,5.6976520664749,333.83329104065));
#32690=CARTESIAN_POINT('Ctrl Pts',(72.287043072518,2.10221600981517,329.577349659575));
#32691=CARTESIAN_POINT('Ctrl Pts',(72.0141287743647,-3.31668618667384,330.283911562685));
#32692=CARTESIAN_POINT('Ctrl Pts',(71.8339604876357,-4.91872723309669,333.464419225402));
#32693=CARTESIAN_POINT('Ctrl Pts',(71.7465382123315,-4.92563732181515,335.001673012725));
#32694=CARTESIAN_POINT('',(75.2465362485451,-4.91824887921523,334.996679668969));
#32695=CARTESIAN_POINT('Ctrl Pts',(75.24653624849,-4.91824887921589,334.996679669946));
#32696=CARTESIAN_POINT('Ctrl Pts',(75.2387502416897,-4.918342051693,335.134691681902));
#32697=CARTESIAN_POINT('Ctrl Pts',(75.2309642348894,-4.91262172361729,335.272740197146));
#32698=CARTESIAN_POINT('Ctrl Pts',(75.2231782280891,-4.90110537645683,335.410303730626));
#32699=CARTESIAN_POINT('Ctrl Pts',(75.215392118815,-4.88958887772644,335.54786907462));
#32700=CARTESIAN_POINT('Ctrl Pts',(75.2076060095409,-4.87227623934469,335.684949040227));
#32701=CARTESIAN_POINT('Ctrl Pts',(75.1998199002667,-4.84923690881224,335.821026470166));
#32702=CARTESIAN_POINT('Ctrl Pts',(75.1920320670668,-4.82619247713191,335.957134029066));
#32703=CARTESIAN_POINT('Ctrl Pts',(75.184244233867,-4.7974188931302,336.092238230602));
#32704=CARTESIAN_POINT('Ctrl Pts',(75.1764564006671,-4.76303683020181,336.225831642862));
#32705=CARTESIAN_POINT('Ctrl Pts',(75.1686652213274,-4.72863999459062,336.3594824552));
#32706=CARTESIAN_POINT('Ctrl Pts',(75.1608740419877,-4.68862997852826,336.49162081324));
#32707=CARTESIAN_POINT('Ctrl Pts',(75.153082862648,-4.6431773670528,336.621754297231));
#32708=CARTESIAN_POINT('Ctrl Pts',(75.1452818525729,-4.59766740449111,336.752051980735));
#32709=CARTESIAN_POINT('Ctrl Pts',(75.1374808424978,-4.5467012589998,336.880339374289));
#32710=CARTESIAN_POINT('Ctrl Pts',(75.1296798324227,-4.49049797789784,337.00614330819));
#32711=CARTESIAN_POINT('Ctrl Pts',(75.1218733667279,-4.43425539115167,337.132035222803));
#32712=CARTESIAN_POINT('Ctrl Pts',(75.1140669010331,-4.3727685424437,337.255439873238));
#32713=CARTESIAN_POINT('Ctrl Pts',(75.1062604353383,-4.30630210015476,337.37590935953));
#32714=CARTESIAN_POINT('Ctrl Pts',(75.0984414107914,-4.23972872827054,337.496572654201));
#32715=CARTESIAN_POINT('Ctrl Pts',(75.0906223862445,-4.16815996133327,337.614291024703));
#32716=CARTESIAN_POINT('Ctrl Pts',(75.0828033616977,-4.09190377840686,337.728645548758));
#32717=CARTESIAN_POINT('Ctrl Pts',(75.0783433795509,-4.04840714882195,337.793873523505));
#32718=CARTESIAN_POINT('Ctrl Pts',(75.0738833974042,-4.00338618302853,337.858007640782));
#32719=CARTESIAN_POINT('Ctrl Pts',(75.0694234152574,-3.95690367396601,337.920975244239));
#32720=CARTESIAN_POINT('Ctrl Pts',(75.061648336479,-3.87587080031553,338.030746553014));
#32721=CARTESIAN_POINT('Ctrl Pts',(75.0538732577005,-3.79013855083957,338.137316779828));
#32722=CARTESIAN_POINT('Ctrl Pts',(75.0460981789221,-3.6999886407755,338.240257261489));
#32723=CARTESIAN_POINT('Ctrl Pts',(75.0383326678731,-3.6099496659151,338.343071068334));
#32724=CARTESIAN_POINT('Ctrl Pts',(75.0305671568241,-3.51550410202622,338.442263726101));
#32725=CARTESIAN_POINT('Ctrl Pts',(75.0228016457751,-3.41697622082204,338.537436440254));
#32726=CARTESIAN_POINT('Ctrl Pts',(75.0150438342529,-3.31854603029906,338.632514790384));
#32727=CARTESIAN_POINT('Ctrl Pts',(75.0072860227307,-3.21604185679651,338.723580859026));
#32728=CARTESIAN_POINT('Ctrl Pts',(74.9995282112085,-3.10982718066701,338.810270065085));
#32729=CARTESIAN_POINT('Ctrl Pts',(74.9917762376856,-3.00369243445,338.896894034767));
#32730=CARTESIAN_POINT('Ctrl Pts',(74.9840242641626,-2.89385304508389,338.979147451715));
#32731=CARTESIAN_POINT('Ctrl Pts',(74.9762722906396,-2.78070790603495,339.056703908817));
#32732=CARTESIAN_POINT('Ctrl Pts',(74.968523600082,-2.66761068401903,339.134227520715));
#32733=CARTESIAN_POINT('Ctrl Pts',(74.9607749095244,-2.55121081852823,339.207057908543));
#32734=CARTESIAN_POINT('Ctrl Pts',(74.9530262189668,-2.43193853489333,339.274910294381));
#32735=CARTESIAN_POINT('Ctrl Pts',(74.945279140589,-2.31269106685314,339.342748562963));
#32736=CARTESIAN_POINT('Ctrl Pts',(74.9375320622111,-2.19057270893039,339.40561069651));
#32737=CARTESIAN_POINT('Ctrl Pts',(74.9297849838333,-2.06604044875218,339.463256650319));
#32738=CARTESIAN_POINT('Ctrl Pts',(74.9220378405275,-1.94150714487402,339.520903087257));
#32739=CARTESIAN_POINT('Ctrl Pts',(74.9142906972217,-1.81456025310254,339.573333093063));
#32740=CARTESIAN_POINT('Ctrl Pts',(74.9065435539159,-1.6856786435854,339.620353944565));
#32741=CARTESIAN_POINT('Ctrl Pts',(74.8987946688878,-1.55676805874611,339.667385367353));
#32742=CARTESIAN_POINT('Ctrl Pts',(74.8910457838597,-1.4259222577556,339.709005082006));
#32743=CARTESIAN_POINT('Ctrl Pts',(74.8832968988316,-1.29363686081873,339.745069729185));
#32744=CARTESIAN_POINT('Ctrl Pts',(74.8755397890569,-1.16121105479461,339.781172655754));
#32745=CARTESIAN_POINT('Ctrl Pts',(74.8677826792822,-1.02734297820329,339.811708633652));
#32746=CARTESIAN_POINT('Ctrl Pts',(74.8600255695074,-0.892540623744539,
339.836584982967));
#32747=CARTESIAN_POINT('Ctrl Pts',(74.8522643145813,-0.757666235217709,
339.861474625409));
#32748=CARTESIAN_POINT('Ctrl Pts',(74.8445030596551,-0.621856960846329,
339.880698558274));
#32749=CARTESIAN_POINT('Ctrl Pts',(74.836741804729,-0.485626590505696,339.894215961428));
#32750=CARTESIAN_POINT('Ctrl Pts',(74.8289681343243,-0.349178295969892,
339.907754988021));
#32751=CARTESIAN_POINT('Ctrl Pts',(74.8211944639196,-0.212307949824023,
339.91556922099));
#32752=CARTESIAN_POINT('Ctrl Pts',(74.813420793515,-0.0755309189842747,
339.917669991244));
#32753=CARTESIAN_POINT('Ctrl Pts',(74.8060089893378,0.0548791081639752,
339.919672970137));
#32754=CARTESIAN_POINT('Ctrl Pts',(74.7985971851607,0.185204024440773,339.916482446133));
#32755=CARTESIAN_POINT('Ctrl Pts',(74.7911853809836,0.315002774085483,339.908152026457));
#32756=CARTESIAN_POINT('Ctrl Pts',(74.7834103022051,0.451163347100028,339.899413308099));
#32757=CARTESIAN_POINT('Ctrl Pts',(74.7756352234267,0.587175163910888,339.884990495225));
#32758=CARTESIAN_POINT('Ctrl Pts',(74.7678601446483,0.722525300214955,339.864888513938));
#32759=CARTESIAN_POINT('Ctrl Pts',(74.7600946335993,0.85770887955958,339.84481126942));
#32760=CARTESIAN_POINT('Ctrl Pts',(74.7523291225502,0.992232015564157,339.819068818629));
#32761=CARTESIAN_POINT('Ctrl Pts',(74.7445636115012,1.12558387136455,339.787718037962));
#32762=CARTESIAN_POINT('Ctrl Pts',(74.736805799979,1.2588035084115,339.756398341685));
#32763=CARTESIAN_POINT('Ctrl Pts',(74.7290479884569,1.39085379831284,339.719481470468));
#32764=CARTESIAN_POINT('Ctrl Pts',(74.7212901769347,1.5212314569717,339.677075786944));
#32765=CARTESIAN_POINT('Ctrl Pts',(74.7135382034117,1.65151100230764,339.634702015042));
#32766=CARTESIAN_POINT('Ctrl Pts',(74.7057862298887,1.78012005158749,339.586847772814));
#32767=CARTESIAN_POINT('Ctrl Pts',(74.6980342563657,1.90656825796609,339.533671860668));
#32768=CARTESIAN_POINT('Ctrl Pts',(74.6902855658081,2.03296291345448,339.480518468553));
#32769=CARTESIAN_POINT('Ctrl Pts',(74.6825368752504,2.15719818658698,339.42204804024));
#32770=CARTESIAN_POINT('Ctrl Pts',(74.6747881846928,2.27880178192222,339.358468251715));
#32771=CARTESIAN_POINT('Ctrl Pts',(74.667041106315,2.40038007661387,339.294901691496));
#32772=CARTESIAN_POINT('Ctrl Pts',(74.6592940279371,2.51932743644053,339.226228066529));
#32773=CARTESIAN_POINT('Ctrl Pts',(74.6515469495593,2.63519470046314,339.152701765496));
#32774=CARTESIAN_POINT('Ctrl Pts',(74.6437998062535,2.75106293556487,339.079174848242));
#32775=CARTESIAN_POINT('Ctrl Pts',(74.6360526629477,2.86385069334135,339.000795383233));
#32776=CARTESIAN_POINT('Ctrl Pts',(74.6283055196419,2.97313676465028,338.917861769025));
#32777=CARTESIAN_POINT('Ctrl Pts',(74.6205566346138,3.0824474057881,338.834909509579));
#32778=CARTESIAN_POINT('Ctrl Pts',(74.6128077495857,3.18825448260362,338.747401299791));
#32779=CARTESIAN_POINT('Ctrl Pts',(74.6050588645576,3.29016923263935,338.6556763373));
#32780=CARTESIAN_POINT('Ctrl Pts',(74.5973017547829,3.39219215604403,338.563854016985));
#32781=CARTESIAN_POINT('Ctrl Pts',(74.5895446450081,3.49031420890693,338.467806265224));
#32782=CARTESIAN_POINT('Ctrl Pts',(74.5817875352334,3.58418255071518,338.367910109497));
#32783=CARTESIAN_POINT('Ctrl Pts',(74.5740262803072,3.67810105276383,338.267960572458));
#32784=CARTESIAN_POINT('Ctrl Pts',(74.5662650253811,3.76776105913171,338.164158829418));
#32785=CARTESIAN_POINT('Ctrl Pts',(74.5585037704549,3.85285020211303,338.056914847126));
#32786=CARTESIAN_POINT('Ctrl Pts',(74.5507301000503,3.93807545999268,337.949499309413));
#32787=CARTESIAN_POINT('Ctrl Pts',(74.5429564296456,4.0187150131237,337.838630845178));
#32788=CARTESIAN_POINT('Ctrl Pts',(74.535182759241,4.09449949529976,337.724748969261));
#32789=CARTESIAN_POINT('Ctrl Pts',(74.5277709550638,4.16675619159799,337.616168322067));
#32790=CARTESIAN_POINT('Ctrl Pts',(74.5203591508867,4.23459950213563,337.504848743999));
#32791=CARTESIAN_POINT('Ctrl Pts',(74.5129473467096,4.29783582579211,337.391190138203));
#32792=CARTESIAN_POINT('Ctrl Pts',(74.5051722679312,4.36417155004215,337.271960785565));
#32793=CARTESIAN_POINT('Ctrl Pts',(74.4973971891527,4.42564689743183,337.149780535497));
#32794=CARTESIAN_POINT('Ctrl Pts',(74.4896221103743,4.48198843765453,337.025083382785));
#32795=CARTESIAN_POINT('Ctrl Pts',(74.4818565993253,4.5382606460251,336.900539677858));
#32796=CARTESIAN_POINT('Ctrl Pts',(74.4740910882763,4.58941145779213,336.773485585642));
#32797=CARTESIAN_POINT('Ctrl Pts',(74.4663255772273,4.6352122583908,336.644381458836));
#32798=CARTESIAN_POINT('Ctrl Pts',(74.4585677657051,4.68096764736237,336.515405339147));
#32799=CARTESIAN_POINT('Ctrl Pts',(74.4508099541829,4.72138345167913,336.384383595895));
#32800=CARTESIAN_POINT('Ctrl Pts',(74.4430521426607,4.75627843988719,336.251798092651));
#32801=CARTESIAN_POINT('Ctrl Pts',(74.4353001691377,4.79114716850988,336.119312364203));
#32802=CARTESIAN_POINT('Ctrl Pts',(74.4275481956148,4.82050325144547,335.985265594564));
#32803=CARTESIAN_POINT('Ctrl Pts',(74.4197962220918,4.84421487253223,335.850156062872));
#32804=CARTESIAN_POINT('Ctrl Pts',(74.4120475315342,4.86791645173343,335.715103750146));
#32805=CARTESIAN_POINT('Ctrl Pts',(74.4042988409766,4.88597825606357,335.578989954733));
#32806=CARTESIAN_POINT('Ctrl Pts',(74.396550150419,4.89831933852613,335.442324225338));
#32807=CARTESIAN_POINT('Ctrl Pts',(74.3888030720411,4.91065785332343,335.30568693039));
#32808=CARTESIAN_POINT('Ctrl Pts',(74.3810559936633,4.91727797860126,335.16849831892));
#32809=CARTESIAN_POINT('Ctrl Pts',(74.3733089152854,4.91815056847279,335.031273764256));
#32810=CARTESIAN_POINT('Ctrl Pts',(74.3655617719796,4.91902316565747,334.894048059519));
#32811=CARTESIAN_POINT('Ctrl Pts',(74.3578146286739,4.91414812887192,334.756786801854));
#32812=CARTESIAN_POINT('Ctrl Pts',(74.3500674853681,4.90354844739205,334.620005675596));
#32813=CARTESIAN_POINT('Ctrl Pts',(74.34231860034,4.89294638287878,334.483193798038));
#32814=CARTESIAN_POINT('Ctrl Pts',(74.3345697153119,4.87661714283574,334.346862656312));
#32815=CARTESIAN_POINT('Ctrl Pts',(74.3268208302838,4.85463558412194,334.21152272837));
#32816=CARTESIAN_POINT('Ctrl Pts',(74.3190637205091,4.83263069395455,334.07603914923));
#32817=CARTESIAN_POINT('Ctrl Pts',(74.3113066107343,4.80496156345587,333.941549271938));
#32818=CARTESIAN_POINT('Ctrl Pts',(74.3035495009596,4.77175430083064,333.808553838814));
#32819=CARTESIAN_POINT('Ctrl Pts',(74.2957882460335,4.73852929330609,333.675487337183));
#32820=CARTESIAN_POINT('Ctrl Pts',(74.2880269911073,4.69976036720641,333.543917245715));
#32821=CARTESIAN_POINT('Ctrl Pts',(74.2802657361812,4.65562323222839,333.414328097608));
#32822=CARTESIAN_POINT('Ctrl Pts',(74.2724920657765,4.61141549221861,333.284531649097));
#32823=CARTESIAN_POINT('Ctrl Pts',(74.2647183953719,4.56182252466442,333.156722840871));
#32824=CARTESIAN_POINT('Ctrl Pts',(74.2569447249672,4.50706815746109,333.031366035419));
#32825=CARTESIAN_POINT('Ctrl Pts',(74.2495329207901,4.45486261922376,332.911844619419));
#32826=CARTESIAN_POINT('Ctrl Pts',(74.2421211166129,4.3979655193077,332.794552321006));
#32827=CARTESIAN_POINT('Ctrl Pts',(74.2347093124358,4.33660837612317,332.679868354029));
#32828=CARTESIAN_POINT('Ctrl Pts',(74.2269342336573,4.27224393657805,332.559563384205));
#32829=CARTESIAN_POINT('Ctrl Pts',(74.2191591548789,4.20276779562158,332.441748709052));
#32830=CARTESIAN_POINT('Ctrl Pts',(74.2113840761004,4.12839693990018,332.326889121431));
#32831=CARTESIAN_POINT('Ctrl Pts',(74.2036185650514,4.05411760225148,332.212170875845));
#32832=CARTESIAN_POINT('Ctrl Pts',(74.1958530540023,3.97495574480711,332.100400807315));
#32833=CARTESIAN_POINT('Ctrl Pts',(74.1880875429533,3.89117477151336,331.992020285966));
#32834=CARTESIAN_POINT('Ctrl Pts',(74.1803297314311,3.80747686729844,331.88374722422));
#32835=CARTESIAN_POINT('Ctrl Pts',(74.1725719199089,3.71916919894507,331.778857328836));
#32836=CARTESIAN_POINT('Ctrl Pts',(74.1648141083867,3.62655890107261,331.67776376524));
#32837=CARTESIAN_POINT('Ctrl Pts',(74.1570621348637,3.53401829538646,331.576746277757));
#32838=CARTESIAN_POINT('Ctrl Pts',(74.1493101613407,3.43718176796271,331.479519722678));
#32839=CARTESIAN_POINT('Ctrl Pts',(74.1415581878177,3.33639699906906,331.386464594458));
#32840=CARTESIAN_POINT('Ctrl Pts',(74.1338094972601,3.23565491258474,331.293448875141));
#32841=CARTESIAN_POINT('Ctrl Pts',(74.1260608067024,3.13096819687038,331.204601333642));
#32842=CARTESIAN_POINT('Ctrl Pts',(74.1183121161448,3.02272153723828,331.12026578606));
#32843=CARTESIAN_POINT('Ctrl Pts',(74.1105650377669,2.91449739922766,331.035947785193));
#32844=CARTESIAN_POINT('Ctrl Pts',(74.1028179593891,2.8027150987018,330.956140151065));
#32845=CARTESIAN_POINT('Ctrl Pts',(74.0950708810112,2.68779225157625,330.881146291155));
#32846=CARTESIAN_POINT('Ctrl Pts',(74.0873237377054,2.57286844128662,330.806151802724));
#32847=CARTESIAN_POINT('Ctrl Pts',(74.0795765943996,2.45480435924134,330.735971382589));
#32848=CARTESIAN_POINT('Ctrl Pts',(74.0718294510938,2.33404609621532,330.670864764963));
#32849=CARTESIAN_POINT('Ctrl Pts',(74.0640805660657,2.21326068416841,330.605743509986));
#32850=CARTESIAN_POINT('Ctrl Pts',(74.0563316810376,2.08978022983497,330.545698512841));
#32851=CARTESIAN_POINT('Ctrl Pts',(74.0485827960095,1.96407451435586,330.490943073706));
#32852=CARTESIAN_POINT('Ctrl Pts',(74.0408256862348,1.8382353735313,330.436129516583));
#32853=CARTESIAN_POINT('Ctrl Pts',(74.0330685764601,1.71016661233389,330.386616889084));
#32854=CARTESIAN_POINT('Ctrl Pts',(74.0253114666853,1.58035756004787,330.342570124532));
#32855=CARTESIAN_POINT('Ctrl Pts',(74.0175502117591,1.4504791419548,330.298499822797));
#32856=CARTESIAN_POINT('Ctrl Pts',(74.009788956833,1.31885895464051,330.25990131387));
#32857=CARTESIAN_POINT('Ctrl Pts',(74.0020277019068,1.18599953900911,330.226889048433));
#32858=CARTESIAN_POINT('Ctrl Pts',(73.9942540315022,1.0529275916114,330.19382397413));
#32859=CARTESIAN_POINT('Ctrl Pts',(73.9864803610975,0.918612837705174,330.166363078767));
#32860=CARTESIAN_POINT('Ctrl Pts',(73.9787066906928,0.783566895731499,330.14456943388));
#32861=CARTESIAN_POINT('Ctrl Pts',(73.9712948865158,0.654807374847598,330.123790288405));
#32862=CARTESIAN_POINT('Ctrl Pts',(73.9638830823387,0.525383493272115,330.108162680669));
#32863=CARTESIAN_POINT('Ctrl Pts',(73.9564712781616,0.395739427918254,330.097697136275));
#32864=CARTESIAN_POINT('Ctrl Pts',(73.9486961993832,0.259741120730986,330.086718644374));
#32865=CARTESIAN_POINT('Ctrl Pts',(73.9409211206048,0.123070720518009,330.081386332583));
#32866=CARTESIAN_POINT('Ctrl Pts',(73.9331460418263,-0.0137634945639107,
330.081769258288));
#32867=CARTESIAN_POINT('Ctrl Pts',(73.9253805307773,-0.150429326432786,
330.082151712779));
#32868=CARTESIAN_POINT('Ctrl Pts',(73.9176150197283,-0.287258184938828,
330.088235410102));
#32869=CARTESIAN_POINT('Ctrl Pts',(73.9098495086793,-0.423736369538326,
330.100037698958));
#32870=CARTESIAN_POINT('Ctrl Pts',(73.9020916971571,-0.560079235619984,
330.111828285811));
#32871=CARTESIAN_POINT('Ctrl Pts',(73.894333885635,-0.696071732813865,330.129326147118));
#32872=CARTESIAN_POINT('Ctrl Pts',(73.8865760741128,-0.831200213334262,
330.152496594343));
#32873=CARTESIAN_POINT('Ctrl Pts',(73.8788241005898,-0.966227005387988,
330.175649605073));
#32874=CARTESIAN_POINT('Ctrl Pts',(73.8710721270668,-1.10039069125888,330.204466639088));
#32875=CARTESIAN_POINT('Ctrl Pts',(73.8633201535439,-1.23318315529974,330.238861232018));
#32876=CARTESIAN_POINT('Ctrl Pts',(73.8555714629862,-1.36591938165324,330.273241258817));
#32877=CARTESIAN_POINT('Ctrl Pts',(73.8478227724287,-1.49728516357397,330.313194048678));
#32878=CARTESIAN_POINT('Ctrl Pts',(73.8400740818711,-1.62678320347397,330.358582170134));
#32879=CARTESIAN_POINT('Ctrl Pts',(73.8323270034932,-1.75625430022562,330.403960848213));
#32880=CARTESIAN_POINT('Ctrl Pts',(73.8245799251154,-1.88385805926641,330.454772479308));
#32881=CARTESIAN_POINT('Ctrl Pts',(73.8168328467375,-2.00911334284012,330.510830072483));
#32882=CARTESIAN_POINT('Ctrl Pts',(73.8090857034317,-2.13436967617367,330.566888135475));
#32883=CARTESIAN_POINT('Ctrl Pts',(73.8013385601259,-2.25727713800847,330.628192088567));
#32884=CARTESIAN_POINT('Ctrl Pts',(73.7935914168201,-2.37737590699044,330.694507361595));
#32885=CARTESIAN_POINT('Ctrl Pts',(73.785842531792,-2.49750167672545,330.760837543704));
#32886=CARTESIAN_POINT('Ctrl Pts',(73.7780936467639,-2.61481715497616,330.832181098757));
#32887=CARTESIAN_POINT('Ctrl Pts',(73.7703447617358,-2.72888874753884,330.908258406735));
#32888=CARTESIAN_POINT('Ctrl Pts',(73.7625876519611,-2.84308141686853,330.984416463954));
#32889=CARTESIAN_POINT('Ctrl Pts',(73.7548305421864,-2.95402299690558,331.065318093699));
#32890=CARTESIAN_POINT('Ctrl Pts',(73.7470734324116,-3.06130998754793,331.150641063419));
#32891=CARTESIAN_POINT('Ctrl Pts',(73.7393121774855,-3.16865430892728,331.236009627005));
#32892=CARTESIAN_POINT('Ctrl Pts',(73.7315509225593,-3.27233985426807,331.325803982548));
#32893=CARTESIAN_POINT('Ctrl Pts',(73.7237896676332,-3.37199842582913,331.419663468512));
#32894=CARTESIAN_POINT('Ctrl Pts',(73.7160159972285,-3.47181641862617,331.513673099065));
#32895=CARTESIAN_POINT('Ctrl Pts',(73.7082423268239,-3.56759429170676,331.611760574918));
#32896=CARTESIAN_POINT('Ctrl Pts',(73.7004686564192,-3.65900214077594,331.713529796834));
#32897=CARTESIAN_POINT('Ctrl Pts',(73.6930568522421,-3.74615493248003,331.810561636987));
#32898=CARTESIAN_POINT('Ctrl Pts',(73.685645048065,-3.8293352098879,331.910939944884));
#32899=CARTESIAN_POINT('Ctrl Pts',(73.6782332438878,-3.90829375218056,332.014296898691));
#32900=CARTESIAN_POINT('Ctrl Pts',(73.6704427153519,-3.99128687533706,332.12293513019));
#32901=CARTESIAN_POINT('Ctrl Pts',(73.662652186816,-4.069880935998,332.235211862015));
#32902=CARTESIAN_POINT('Ctrl Pts',(73.6548616582801,-4.14374063615689,332.350736592416));
#32903=CARTESIAN_POINT('Ctrl Pts',(73.647080635971,-4.21751021058738,332.466120356222));
#32904=CARTESIAN_POINT('Ctrl Pts',(73.6392996136619,-4.28655670949134,332.584743910954));
#32905=CARTESIAN_POINT('Ctrl Pts',(73.6315185913527,-4.35058515732752,332.706183997932));
#32906=CARTESIAN_POINT('Ctrl Pts',(73.6237454044059,-4.41454912956359,332.827501796728));
#32907=CARTESIAN_POINT('Ctrl Pts',(73.615972217459,-4.47350492478126,332.951630143701));
#32908=CARTESIAN_POINT('Ctrl Pts',(73.6081990305121,-4.52720116778406,333.078117420623));
#32909=CARTESIAN_POINT('Ctrl Pts',(73.6004320138054,-4.58085478750822,333.204504293826));
#32910=CARTESIAN_POINT('Ctrl Pts',(73.5926649970986,-4.62925701260594,333.333246014631));
#32911=CARTESIAN_POINT('Ctrl Pts',(73.5848979803918,-4.67220285223906,333.463867333194));
#32912=CARTESIAN_POINT('Ctrl Pts',(73.5771352940564,-4.71512474813176,333.594415826007));
#32913=CARTESIAN_POINT('Ctrl Pts',(73.5693726077209,-4.75259619253078,333.72684146275));
#32914=CARTESIAN_POINT('Ctrl Pts',(73.5616099213855,-4.78446082557265,333.860650329767));
#32915=CARTESIAN_POINT('Ctrl Pts',(73.5538498962635,-4.81631453474276,333.994413324267));
#32916=CARTESIAN_POINT('Ctrl Pts',(73.5460898711415,-4.84256517022996,334.129558227385));
#32917=CARTESIAN_POINT('Ctrl Pts',(73.5383298460195,-4.863106713813,334.265577674245));
#32918=CARTESIAN_POINT('Ctrl Pts',(73.5305691113377,-4.88365013566995,334.401609558427));
#32919=CARTESIAN_POINT('Ctrl Pts',(73.522808376656,-4.89848335773919,334.538515763089));
#32920=CARTESIAN_POINT('Ctrl Pts',(73.5150476419742,-4.90755181097736,334.675780498623));
#32921=CARTESIAN_POINT('Ctrl Pts',(73.5088771774795,-4.91476202637872,334.784917998065));
#32922=CARTESIAN_POINT('Ctrl Pts',(73.5027067129847,-4.91832896017515,334.89428191533));
#32923=CARTESIAN_POINT('Ctrl Pts',(73.49653624849,-4.91824867386945,335.003611714461));
#32924=CARTESIAN_POINT('',(76.9965362484552,-4.91824952845184,334.997846309397));
#32925=CARTESIAN_POINT('Ctrl Pts',(76.9965362484552,-4.91824952845184,334.997846309397));
#32926=CARTESIAN_POINT('Ctrl Pts',(76.9888439017237,-4.91830869035386,335.132950672227));
#32927=CARTESIAN_POINT('Ctrl Pts',(76.9811515549923,-4.91279667151199,335.268281913705));
#32928=CARTESIAN_POINT('Ctrl Pts',(76.9734592082608,-4.90168365733435,335.403336566556));
#32929=CARTESIAN_POINT('Ctrl Pts',(76.9657758500902,-4.89058362879128,335.538233407103));
#32930=CARTESIAN_POINT('Ctrl Pts',(76.9580924919196,-4.87389565485011,335.672853907188));
#32931=CARTESIAN_POINT('Ctrl Pts',(76.9504091337489,-4.85164191001208,335.806693150779));
#32932=CARTESIAN_POINT('Ctrl Pts',(76.942732822733,-4.82940857624697,335.940409637389));
#32933=CARTESIAN_POINT('Ctrl Pts',(76.9350565117171,-4.80161969232445,336.073345901045));
#32934=CARTESIAN_POINT('Ctrl Pts',(76.9273802007013,-4.7683493178205,336.205001180805));
#32935=CARTESIAN_POINT('Ctrl Pts',(76.9195248432096,-4.73430292690824,336.339727260303));
#32936=CARTESIAN_POINT('Ctrl Pts',(76.9116694857179,-4.69451620765234,336.473111436587));
#32937=CARTESIAN_POINT('Ctrl Pts',(76.9038141282262,-4.64912427591835,336.60462660129));
#32938=CARTESIAN_POINT('Ctrl Pts',(76.8961452572008,-4.60480995025813,336.733019591305));
#32939=CARTESIAN_POINT('Ctrl Pts',(76.8884763861754,-4.55515370478375,336.859630918255));
#32940=CARTESIAN_POINT('Ctrl Pts',(76.88080751515,-4.50033184766666,336.983984960472));
#32941=CARTESIAN_POINT('Ctrl Pts',(76.8731394257967,-4.44551557842832,337.108326327538));
#32942=CARTESIAN_POINT('Ctrl Pts',(76.8654713364435,-4.38553490576362,337.230410501663));
#32943=CARTESIAN_POINT('Ctrl Pts',(76.8578032470902,-4.32061407250618,337.349782351402));
#32944=CARTESIAN_POINT('Ctrl Pts',(76.8501341961009,-4.25568509768783,337.469169171269));
#32945=CARTESIAN_POINT('Ctrl Pts',(76.8424651451115,-4.18581492134049,337.585842639204));
#32946=CARTESIAN_POINT('Ctrl Pts',(76.8347960941222,-4.11127322269474,337.699373177398));
#32947=CARTESIAN_POINT('Ctrl Pts',(76.8268007213537,-4.03355973920203,337.817734494166));
#32948=CARTESIAN_POINT('Ctrl Pts',(76.8188053485854,-3.95076867280854,337.932679113518));
#32949=CARTESIAN_POINT('Ctrl Pts',(76.8108099758169,-3.86325422535034,338.043755879306));
#32950=CARTESIAN_POINT('Ctrl Pts',(76.8031295868382,-3.77918747609316,338.150456691447));
#32951=CARTESIAN_POINT('Ctrl Pts',(76.7954491978594,-3.69076274249829,338.253588344619));
#32952=CARTESIAN_POINT('Ctrl Pts',(76.7877688088806,-3.59833303777858,338.352787260136));
#32953=CARTESIAN_POINT('Ctrl Pts',(76.7800832160429,-3.50584070717496,338.452053388026));
#32954=CARTESIAN_POINT('Ctrl Pts',(76.7723976232051,-3.4093382867939,338.547381194029));
#32955=CARTESIAN_POINT('Ctrl Pts',(76.7647120303674,-3.30921333392912,338.638446120674));
#32956=CARTESIAN_POINT('Ctrl Pts',(76.7570159573274,-3.20895184901355,338.729635224967));
#32957=CARTESIAN_POINT('Ctrl Pts',(76.7493198842875,-3.10505828171344,338.816549598504));
#32958=CARTESIAN_POINT('Ctrl Pts',(76.7416238112475,-2.99795082777614,338.89890675661));
#32959=CARTESIAN_POINT('Ctrl Pts',(76.7406997477987,-2.98509049202248,338.908795337339));
#32960=CARTESIAN_POINT('Ctrl Pts',(76.7397756843499,-2.97218385344695,338.918618271675));
#32961=CARTESIAN_POINT('Ctrl Pts',(76.7388516209011,-2.9592316603781,338.928375114817));
#32962=CARTESIAN_POINT('Ctrl Pts',(76.7310765421227,-2.85025178286683,339.010469287204));
#32963=CARTESIAN_POINT('Ctrl Pts',(76.7233014633442,-2.73768095754818,339.088154814366));
#32964=CARTESIAN_POINT('Ctrl Pts',(76.7155263845658,-2.62191147708508,339.161101208674));
#32965=CARTESIAN_POINT('Ctrl Pts',(76.7077608735168,-2.50628445833817,339.2339578378));
#32966=CARTESIAN_POINT('Ctrl Pts',(76.6999953624678,-2.3874669437934,339.302086731307));
#32967=CARTESIAN_POINT('Ctrl Pts',(76.6922298514188,-2.26588349377321,339.365198169058));
#32968=CARTESIAN_POINT('Ctrl Pts',(76.6844720398966,-2.14442059409745,339.428247031635));
#32969=CARTESIAN_POINT('Ctrl Pts',(76.6767142283744,-2.02019756122928,339.486288159712));
#32970=CARTESIAN_POINT('Ctrl Pts',(76.6689564168522,-1.89366677500193,339.539075809871));
#32971=CARTESIAN_POINT('Ctrl Pts',(76.6612044433292,-1.76723120720391,339.591823735648));
#32972=CARTESIAN_POINT('Ctrl Pts',(76.6534524698062,-1.63849170206592,339.639325902681));
#32973=CARTESIAN_POINT('Ctrl Pts',(76.6457004962832,-1.5079236913063,339.68138325751));
#32974=CARTESIAN_POINT('Ctrl Pts',(76.6379518057255,-1.37741097617676,339.723422801024));
#32975=CARTESIAN_POINT('Ctrl Pts',(76.6302031151679,-1.24507166687453,339.760021998978));
#32976=CARTESIAN_POINT('Ctrl Pts',(76.6224544246103,-1.11139934968372,339.791030635262));
#32977=CARTESIAN_POINT('Ctrl Pts',(76.6147073462325,-0.977754844134961,
339.822032819941));
#32978=CARTESIAN_POINT('Ctrl Pts',(76.6069602678546,-0.842778262877886,
339.847446668292));
#32979=CARTESIAN_POINT('Ctrl Pts',(76.5992131894768,-0.706976081593008,
339.867172473064));
#32980=CARTESIAN_POINT('Ctrl Pts',(76.591466046171,-0.571172762155234,339.886898443158));
#32981=CARTESIAN_POINT('Ctrl Pts',(76.5837189028652,-0.434544215703492,
339.900936218402));
#32982=CARTESIAN_POINT('Ctrl Pts',(76.5759717595594,-0.297604391943369,
339.909237689132));
#32983=CARTESIAN_POINT('Ctrl Pts',(76.5682228745314,-0.160633781203643,
339.917541026209));
#32984=CARTESIAN_POINT('Ctrl Pts',(76.5604739895033,-0.0233521439814797,
339.920105468879));
#32985=CARTESIAN_POINT('Ctrl Pts',(76.5527251044752,0.113724597793962,339.916934998386));
#32986=CARTESIAN_POINT('Ctrl Pts',(76.5449679947005,0.250946834239485,339.913761162724));
#32987=CARTESIAN_POINT('Ctrl Pts',(76.5372108849257,0.387963349418304,339.904840263406));
#32988=CARTESIAN_POINT('Ctrl Pts',(76.529453775151,0.524260820138937,339.890228384745));
#32989=CARTESIAN_POINT('Ctrl Pts',(76.5216925202248,0.660631123870345,339.875608697963));
#32990=CARTESIAN_POINT('Ctrl Pts',(76.5139312652987,0.796281231155387,339.855292030084));
#32991=CARTESIAN_POINT('Ctrl Pts',(76.5061700103725,0.930707056357455,339.829385824072));
#32992=CARTESIAN_POINT('Ctrl Pts',(76.4983963399678,1.0653479190703,339.803438176573));
#32993=CARTESIAN_POINT('Ctrl Pts',(76.4906226695632,1.198760205553,339.771883213311));
#32994=CARTESIAN_POINT('Ctrl Pts',(76.4828489991585,1.3304531955942,339.734878811209));
#32995=CARTESIAN_POINT('Ctrl Pts',(76.4754371949814,1.45601584526583,339.699596972926));
#32996=CARTESIAN_POINT('Ctrl Pts',(76.4680253908043,1.58001538905194,339.659361709951));
#32997=CARTESIAN_POINT('Ctrl Pts',(76.4606135866272,1.70204439015038,339.614350220395));
#32998=CARTESIAN_POINT('Ctrl Pts',(76.4528385078487,1.83005439609802,339.567132583653));
#32999=CARTESIAN_POINT('Ctrl Pts',(76.4450634290703,1.95630034612933,339.514509471391));
#33000=CARTESIAN_POINT('Ctrl Pts',(76.4372883502919,2.08029203407565,339.45663192506));
#33001=CARTESIAN_POINT('Ctrl Pts',(76.4295228392429,2.20413114235634,339.398825600733));
#33002=CARTESIAN_POINT('Ctrl Pts',(76.4217573281938,2.32572115724088,339.335777871404));
#33003=CARTESIAN_POINT('Ctrl Pts',(76.4139918171448,2.4445886929321,339.267688974713));
#33004=CARTESIAN_POINT('Ctrl Pts',(76.4062340056226,2.5633383711152,339.199667588362));
#33005=CARTESIAN_POINT('Ctrl Pts',(76.3984761941004,2.67937060496968,339.126615174643));
#33006=CARTESIAN_POINT('Ctrl Pts',(76.3907183825783,2.79223393492516,339.048779163545));
#33007=CARTESIAN_POINT('Ctrl Pts',(76.3829664090552,2.90501233164598,338.971001726512));
#33008=CARTESIAN_POINT('Ctrl Pts',(76.3752144355323,3.01462625061978,338.88844807836));
#33009=CARTESIAN_POINT('Ctrl Pts',(76.3674624620093,3.12065102016262,338.801410300515));
#33010=CARTESIAN_POINT('Ctrl Pts',(76.3597137714517,3.22663088815254,338.71440938322));
#33011=CARTESIAN_POINT('Ctrl Pts',(76.351965080894,3.32902432841263,338.622928360766));
#33012=CARTESIAN_POINT('Ctrl Pts',(76.3442163903364,3.42743791315231,338.527301009835));
#33013=CARTESIAN_POINT('Ctrl Pts',(76.3364693119586,3.52583102212385,338.431693554974));
#33014=CARTESIAN_POINT('Ctrl Pts',(76.3287222335807,3.62024564245577,338.331941759784));
#33015=CARTESIAN_POINT('Ctrl Pts',(76.3209751552029,3.71032384514119,338.228417573158));
#33016=CARTESIAN_POINT('Ctrl Pts',(76.3132280118971,3.80040280276851,338.1248925189));
#33017=CARTESIAN_POINT('Ctrl Pts',(76.3054808685913,3.88614501368369,338.017595305018));
#33018=CARTESIAN_POINT('Ctrl Pts',(76.2977337252855,3.9672318937667,337.906932087886));
#33019=CARTESIAN_POINT('Ctrl Pts',(76.2899848402574,4.04833700390194,337.796243991313));
#33020=CARTESIAN_POINT('Ctrl Pts',(76.2822359552293,4.12478446957256,337.682188700873));
#33021=CARTESIAN_POINT('Ctrl Pts',(76.2744870702012,4.19629844373307,337.565202220805));
#33022=CARTESIAN_POINT('Ctrl Pts',(76.2667299604265,4.26788832356468,337.448091570078));
#33023=CARTESIAN_POINT('Ctrl Pts',(76.2589728506517,4.3345340473788,337.328043848843));
#33024=CARTESIAN_POINT('Ctrl Pts',(76.251215740877,4.39600498903616,337.205521071962));
#33025=CARTESIAN_POINT('Ctrl Pts',(76.2434544859508,4.45750877879925,337.082932822827));
#33026=CARTESIAN_POINT('Ctrl Pts',(76.2356932310247,4.51383211599612,336.957867238883));
#33027=CARTESIAN_POINT('Ctrl Pts',(76.2279319760985,4.56479256204452,336.830806360051));
#33028=CARTESIAN_POINT('Ctrl Pts',(76.2201583056939,4.61583452819862,336.703542225221));
#33029=CARTESIAN_POINT('Ctrl Pts',(76.2123846352892,4.66149632980786,336.574276786048));
#33030=CARTESIAN_POINT('Ctrl Pts',(76.2046109648846,4.70164517207886,336.443508135885));
#33031=CARTESIAN_POINT('Ctrl Pts',(76.1971991607075,4.73992507608306,336.318826797849));
#33032=CARTESIAN_POINT('Ctrl Pts',(76.1897873565303,4.77319365330056,336.19277932657));
#33033=CARTESIAN_POINT('Ctrl Pts',(76.1823755523532,4.80137942597151,336.065804236414));
#33034=CARTESIAN_POINT('Ctrl Pts',(76.1746004735748,4.83094666732211,335.93260571885));
#33035=CARTESIAN_POINT('Ctrl Pts',(76.1668253947963,4.85501369710965,335.797965420571));
#33036=CARTESIAN_POINT('Ctrl Pts',(76.1590503160179,4.87344225062529,335.662377303597));
#33037=CARTESIAN_POINT('Ctrl Pts',(76.1512848049688,4.89184812663258,335.526956036433));
#33038=CARTESIAN_POINT('Ctrl Pts',(76.1435192939198,4.90462927986278,335.390589654889));
#33039=CARTESIAN_POINT('Ctrl Pts',(76.1357537828708,4.9116979182029,335.25378459926));
#33040=CARTESIAN_POINT('Ctrl Pts',(76.1279959713486,4.91875954796753,335.117115186241));
#33041=CARTESIAN_POINT('Ctrl Pts',(76.1202381598264,4.92011991443344,334.980008352543));
#33042=CARTESIAN_POINT('Ctrl Pts',(76.1124803483042,4.91574277607731,334.842977638714));
#33043=CARTESIAN_POINT('Ctrl Pts',(76.1047283747811,4.91136893165659,334.706050044843));
#33044=CARTESIAN_POINT('Ctrl Pts',(76.0969764012581,4.90126618892265,334.569198845924));
#33045=CARTESIAN_POINT('Ctrl Pts',(76.089224427735,4.88545035116212,334.432939219457));
#33046=CARTESIAN_POINT('Ctrl Pts',(76.0814757371774,4.86964121141834,334.296737299023));
#33047=CARTESIAN_POINT('Ctrl Pts',(76.0737270466198,4.84812383383427,334.16112684021));
#33048=CARTESIAN_POINT('Ctrl Pts',(76.0659783560622,4.82096599198929,334.026619310556));
#33049=CARTESIAN_POINT('Ctrl Pts',(76.0582312776844,4.79381380056013,333.892139766316));
#33050=CARTESIAN_POINT('Ctrl Pts',(76.0504841993065,4.76102355644561,333.758763077698));
#33051=CARTESIAN_POINT('Ctrl Pts',(76.0427371209287,4.72271434347904,333.626991517726));
#33052=CARTESIAN_POINT('Ctrl Pts',(76.0349899776229,4.68440480944441,333.495218853381));
#33053=CARTESIAN_POINT('Ctrl Pts',(76.0272428343171,4.64057632341896,333.365051719848));
#33054=CARTESIAN_POINT('Ctrl Pts',(76.0194956910113,4.59139802681291,333.236977815829));
#33055=CARTESIAN_POINT('Ctrl Pts',(76.0117468059832,4.54220867388169,333.108875118077));
#33056=CARTESIAN_POINT('Ctrl Pts',(76.0039979209551,4.48766725711725,332.982866951112));
#33057=CARTESIAN_POINT('Ctrl Pts',(75.996249035927,4.42799114511993,332.859421227509));
#33058=CARTESIAN_POINT('Ctrl Pts',(75.9884919261522,4.36825169228073,332.735844477339));
#33059=CARTESIAN_POINT('Ctrl Pts',(75.9807348163775,4.30336682767488,332.614835956063));
#33060=CARTESIAN_POINT('Ctrl Pts',(75.9729777066028,4.2336002644193,332.496839624872));
#33061=CARTESIAN_POINT('Ctrl Pts',(75.9652164516766,4.16379642014307,332.378780240215));
#33062=CARTESIAN_POINT('Ctrl Pts',(75.9574551967504,4.08910589203741,332.263736580627));
#33063=CARTESIAN_POINT('Ctrl Pts',(75.9496939418243,4.0098353097686,332.152122922064));
#33064=CARTESIAN_POINT('Ctrl Pts',(75.9419202714196,3.93043792040227,332.040330718022));
#33065=CARTESIAN_POINT('Ctrl Pts',(75.934146601015,3.84644607576806,331.93197978851));
#33066=CARTESIAN_POINT('Ctrl Pts',(75.9263729306103,3.75820677031242,331.8274513504));
#33067=CARTESIAN_POINT('Ctrl Pts',(75.9189611264333,3.67407502575632,331.727788736234));
#33068=CARTESIAN_POINT('Ctrl Pts',(75.9115493222563,3.58608255413759,331.631600960588));
#33069=CARTESIAN_POINT('Ctrl Pts',(75.9041375180794,3.49455943082387,331.539185435921));
#33070=CARTESIAN_POINT('Ctrl Pts',(75.8963624393009,3.39855048660167,331.442240351097));
#33071=CARTESIAN_POINT('Ctrl Pts',(75.8885873605225,3.29835263813812,331.349140281244));
#33072=CARTESIAN_POINT('Ctrl Pts',(75.8808122817441,3.19430644566673,331.260268807298));
#33073=CARTESIAN_POINT('Ctrl Pts',(75.8730467706951,3.09038828865901,331.171506695358));
#33074=CARTESIAN_POINT('Ctrl Pts',(75.865281259646,2.98263150456502,331.086963077178));
#33075=CARTESIAN_POINT('Ctrl Pts',(75.857515748597,2.87141446048222,331.006985842921));
#33076=CARTESIAN_POINT('Ctrl Pts',(75.8497579370748,2.76030768842282,330.927087906325));
#33077=CARTESIAN_POINT('Ctrl Pts',(75.8420001255527,2.64574779927336,330.85174757024));
#33078=CARTESIAN_POINT('Ctrl Pts',(75.8342423140305,2.52814702786863,330.781273217192));
#33079=CARTESIAN_POINT('Ctrl Pts',(75.8264903405075,2.41063475477339,330.71085189833));
#33080=CARTESIAN_POINT('Ctrl Pts',(75.8187383669845,2.29008648822242,330.645289473973));
#33081=CARTESIAN_POINT('Ctrl Pts',(75.8109863934614,2.16694400403005,330.584851446905));
#33082=CARTESIAN_POINT('Ctrl Pts',(75.8032377029038,2.04385367075301,330.524439015377));
#33083=CARTESIAN_POINT('Ctrl Pts',(75.7954890123462,1.91817165513783,330.469146836651));
#33084=CARTESIAN_POINT('Ctrl Pts',(75.7877403217886,1.79036473732038,330.419194702909));
#33085=CARTESIAN_POINT('Ctrl Pts',(75.7799932434108,1.66258441079965,330.369252962125));
#33086=CARTESIAN_POINT('Ctrl Pts',(75.772246165033,1.53268042527964,330.324649198586));
#33087=CARTESIAN_POINT('Ctrl Pts',(75.7644990866551,1.40113959595773,330.285555080909));
#33088=CARTESIAN_POINT('Ctrl Pts',(75.7567519433493,1.26959766419688,330.246460635586));
#33089=CARTESIAN_POINT('Ctrl Pts',(75.7490048000435,1.13641923594893,330.212876039581));
#33090=CARTESIAN_POINT('Ctrl Pts',(75.7412576567377,1.00210595957867,330.184922980026));
#33091=CARTESIAN_POINT('Ctrl Pts',(75.7335087717096,0.867762486732522,330.15696363603));
#33092=CARTESIAN_POINT('Ctrl Pts',(75.7257598866815,0.732284040667951,330.134638427485));
#33093=CARTESIAN_POINT('Ctrl Pts',(75.7180110016534,0.596181729674974,330.118017778842));
#33094=CARTESIAN_POINT('Ctrl Pts',(75.7102538918787,0.45993495828263,330.101379488871));
#33095=CARTESIAN_POINT('Ctrl Pts',(75.7024967821039,0.323063387806579,330.090457901445));
#33096=CARTESIAN_POINT('Ctrl Pts',(75.6947396723292,0.186083064984924,330.085271507456));
#33097=CARTESIAN_POINT('Ctrl Pts',(75.686978417403,0.0490295442586284,330.080082342023));
#33098=CARTESIAN_POINT('Ctrl Pts',(75.6792171624768,-0.0881324539373592,
330.080634475153));
#33099=CARTESIAN_POINT('Ctrl Pts',(75.6714559075507,-0.224888621207158,
330.086894243907));
#33100=CARTESIAN_POINT('Ctrl Pts',(75.663682237146,-0.361863553775857,330.093164026252));
#33101=CARTESIAN_POINT('Ctrl Pts',(75.6559085667414,-0.498430968550139,
330.105159655158));
#33102=CARTESIAN_POINT('Ctrl Pts',(75.6481348963367,-0.634082513525635,
330.122795633917));
#33103=CARTESIAN_POINT('Ctrl Pts',(75.6407230921596,-0.763419446447297,
330.139610653621));
#33104=CARTESIAN_POINT('Ctrl Pts',(75.6333112879824,-0.891923574466551,
330.161552675588));
#33105=CARTESIAN_POINT('Ctrl Pts',(75.6258994838053,-1.01916617438121,330.188505079344));
#33106=CARTESIAN_POINT('Ctrl Pts',(75.6181244050268,-1.15264531315326,330.216778500696));
#33107=CARTESIAN_POINT('Ctrl Pts',(75.6103493262484,-1.28515795325081,330.250655219218));
#33108=CARTESIAN_POINT('Ctrl Pts',(75.6025742474699,-1.4161972365976,330.290056428199));
#33109=CARTESIAN_POINT('Ctrl Pts',(75.5948087364209,-1.54707526776422,330.329409151484));
#33110=CARTESIAN_POINT('Ctrl Pts',(75.5870432253718,-1.67648317890724,330.37427272721));
#33111=CARTESIAN_POINT('Ctrl Pts',(75.5792777143228,-1.80392366561939,330.424517241742));
#33112=CARTESIAN_POINT('Ctrl Pts',(75.5715199028006,-1.93123779471751,330.474711938691));
#33113=CARTESIAN_POINT('Ctrl Pts',(75.5637620912784,-2.05658802011141,330.530276814622));
#33114=CARTESIAN_POINT('Ctrl Pts',(75.5560042797562,-2.17949193243152,330.591032095947));
#33115=CARTESIAN_POINT('Ctrl Pts',(75.5482523062331,-2.30230335566078,330.651741656997));
#33116=CARTESIAN_POINT('Ctrl Pts',(75.5405003327101,-2.42267178110516,330.717633676334));
#33117=CARTESIAN_POINT('Ctrl Pts',(75.532748359187,-2.54013487156683,330.788480334042));
#33118=CARTESIAN_POINT('Ctrl Pts',(75.5249996686294,-2.6575482163394,330.859296988148));
#33119=CARTESIAN_POINT('Ctrl Pts',(75.5172509780717,-2.77205833931942,330.935063905814));
#33120=CARTESIAN_POINT('Ctrl Pts',(75.5095022875141,-2.88322781105554,331.015507503827));
#33121=CARTESIAN_POINT('Ctrl Pts',(75.5017552091363,-2.99437415305456,331.095934364878));
#33122=CARTESIAN_POINT('Ctrl Pts',(75.4940081307584,-3.10218090984829,331.181035741868));
#33123=CARTESIAN_POINT('Ctrl Pts',(75.4862610523806,-3.20624027799651,331.270495161251));
#33124=CARTESIAN_POINT('Ctrl Pts',(75.4785139090748,-3.31030051826226,331.35995533039));
#33125=CARTESIAN_POINT('Ctrl Pts',(75.470766765769,-3.41061301083981,331.453773359959));
#33126=CARTESIAN_POINT('Ctrl Pts',(75.4630196224632,-3.50680395570985,331.551593255035));
#33127=CARTESIAN_POINT('Ctrl Pts',(75.4552707374351,-3.60301652634654,331.649435142101));
#33128=CARTESIAN_POINT('Ctrl Pts',(75.447521852407,-3.69510543141647,331.751280406339));
#33129=CARTESIAN_POINT('Ctrl Pts',(75.4397729673789,-3.78273485947376,331.856737356596));
#33130=CARTESIAN_POINT('Ctrl Pts',(75.4320158576041,-3.87045729831131,331.962306239948));
#33131=CARTESIAN_POINT('Ctrl Pts',(75.4242587478294,-3.95371055465251,332.071494165952));
#33132=CARTESIAN_POINT('Ctrl Pts',(75.4165016380547,-4.03219981661281,332.183877186377));
#33133=CARTESIAN_POINT('Ctrl Pts',(75.4087403831285,-4.11073102072511,332.296320260695));
#33134=CARTESIAN_POINT('Ctrl Pts',(75.4009791282023,-4.18449294777455,332.411961502119));
#33135=CARTESIAN_POINT('Ctrl Pts',(75.3932178732762,-4.25323558385935,332.530350200799));
#33136=CARTESIAN_POINT('Ctrl Pts',(75.3854442028715,-4.32208818575875,332.648928282815));
#33137=CARTESIAN_POINT('Ctrl Pts',(75.3776705324668,-4.38590526986643,332.770262258547));
#33138=CARTESIAN_POINT('Ctrl Pts',(75.3698968620621,-4.44448363375122,332.893878376775));
#33139=CARTESIAN_POINT('Ctrl Pts',(75.3624850578852,-4.50033516070281,333.011740134956));
#33140=CARTESIAN_POINT('Ctrl Pts',(75.3550732537083,-4.55142460355379,333.131676084838));
#33141=CARTESIAN_POINT('Ctrl Pts',(75.3476614495313,-4.59761802422218,333.253262593906));
#33142=CARTESIAN_POINT('Ctrl Pts',(75.3387749079294,-4.65300261678632,333.399041346997));
#33143=CARTESIAN_POINT('Ctrl Pts',(75.3298883663275,-4.7014951093337,333.547575031307));
#33144=CARTESIAN_POINT('Ctrl Pts',(75.3210018247256,-4.74284895472082,333.698244702256));
#33145=CARTESIAN_POINT('Ctrl Pts',(75.3121462132614,-4.78405886558402,333.848389958435));
#33146=CARTESIAN_POINT('Ctrl Pts',(75.3032906017973,-4.81817963094701,334.000656207855));
#33147=CARTESIAN_POINT('Ctrl Pts',(75.2944349903331,-4.84501377317844,334.154408727451));
#33148=CARTESIAN_POINT('Ctrl Pts',(75.2856386784745,-4.87166822662651,334.307131677965));
#33149=CARTESIAN_POINT('Ctrl Pts',(75.2768423666159,-4.89113323208053,334.46132089513));
#33150=CARTESIAN_POINT('Ctrl Pts',(75.2680460547573,-4.90326258944528,334.616334727339));
#33151=CARTESIAN_POINT('Ctrl Pts',(75.2608761193532,-4.91314931358559,334.742687587667));
#33152=CARTESIAN_POINT('Ctrl Pts',(75.2537061839492,-4.91816307902829,334.869587921416));
#33153=CARTESIAN_POINT('Ctrl Pts',(75.2465362485452,-4.91824887921523,334.996679668969));
#33154=CARTESIAN_POINT('',(78.7465362485187,-4.9182479660083,335.004472958214));
#33155=CARTESIAN_POINT('Ctrl Pts',(78.74653624849,-4.91824796600784,335.004472958721));
#33156=CARTESIAN_POINT('Ctrl Pts',(78.7357876945031,-4.91807550825578,335.194099119235));
#33157=CARTESIAN_POINT('Ctrl Pts',(78.7250391405163,-4.90693287809721,335.383246192589));
#33158=CARTESIAN_POINT('Ctrl Pts',(78.7142905865295,-4.88500627415459,335.570873684777));
#33159=CARTESIAN_POINT('Ctrl Pts',(78.7050330112925,-4.86612120496873,335.732474550118));
#33160=CARTESIAN_POINT('Ctrl Pts',(78.6957754360556,-4.83923724108489,335.892949057504));
#33161=CARTESIAN_POINT('Ctrl Pts',(78.6865178608187,-4.80449992880622,336.051647990823));
#33162=CARTESIAN_POINT('Ctrl Pts',(78.6787427820402,-4.77532540603914,336.184933076498));
#33163=CARTESIAN_POINT('Ctrl Pts',(78.6709677032617,-4.7405542433559,336.317213831293));
#33164=CARTESIAN_POINT('Ctrl Pts',(78.6631926244833,-4.70026866985679,336.447983941093));
#33165=CARTESIAN_POINT('Ctrl Pts',(78.6554271134343,-4.66003267032059,336.578593129947));
#33166=CARTESIAN_POINT('Ctrl Pts',(78.6476616023853,-4.61429587580899,336.707695002594));
#33167=CARTESIAN_POINT('Ctrl Pts',(78.6398960913363,-4.56319155663783,336.834793143635));
#33168=CARTESIAN_POINT('Ctrl Pts',(78.632138279814,-4.51213790754781,336.961765266499));
#33169=CARTESIAN_POINT('Ctrl Pts',(78.6243804682918,-4.45572746959211,337.086737251092));
#33170=CARTESIAN_POINT('Ctrl Pts',(78.6166226567696,-4.39414327127363,337.209227913553));
#33171=CARTESIAN_POINT('Ctrl Pts',(78.6088706832466,-4.33260541701741,337.331626397905));
#33172=CARTESIAN_POINT('Ctrl Pts',(78.6011187097236,-4.26590172692788,337.451546929027));
#33173=CARTESIAN_POINT('Ctrl Pts',(78.5933667362005,-4.19426313913914,337.568528719356));
#33174=CARTESIAN_POINT('Ctrl Pts',(78.5856180456429,-4.12265489033486,337.685460967828));
#33175=CARTESIAN_POINT('Ctrl Pts',(78.5778693550853,-4.04611610426616,337.799456618204));
#33176=CARTESIAN_POINT('Ctrl Pts',(78.5701206645277,-3.96492331304977,337.910080099264));
#33177=CARTESIAN_POINT('Ctrl Pts',(78.5623735861498,-3.88374741467179,338.020680564186));
#33178=CARTESIAN_POINT('Ctrl Pts',(78.554626507772,-3.79791966830381,338.127909940428));
#33179=CARTESIAN_POINT('Ctrl Pts',(78.5468794293942,-3.70775929527203,338.231362571861));
#33180=CARTESIAN_POINT('Ctrl Pts',(78.5391322860883,-3.61759816660949,338.334816070327));
#33181=CARTESIAN_POINT('Ctrl Pts',(78.5313851427826,-3.52310459566713,338.434492466179));
#33182=CARTESIAN_POINT('Ctrl Pts',(78.5236379994767,-3.42463709452955,338.530020372926));
#33183=CARTESIAN_POINT('Ctrl Pts',(78.5158891144486,-3.32614745580719,338.625569756375));
#33184=CARTESIAN_POINT('Ctrl Pts',(78.5081402294205,-3.22368238956685,338.716968522696));
#33185=CARTESIAN_POINT('Ctrl Pts',(78.5003913443924,-3.11763584666953,338.80388351426));
#33186=CARTESIAN_POINT('Ctrl Pts',(78.4926342346176,-3.01147674487592,338.890890758294));
#33187=CARTESIAN_POINT('Ctrl Pts',(78.4848771248429,-2.90172887552791,338.973404472609));
#33188=CARTESIAN_POINT('Ctrl Pts',(78.4771200150681,-2.78881816884506,339.05113271612));
#33189=CARTESIAN_POINT('Ctrl Pts',(78.469358760142,-2.67584712629082,339.128902495119));
#33190=CARTESIAN_POINT('Ctrl Pts',(78.4615975052158,-2.55971020947508,339.201881499995));
#33191=CARTESIAN_POINT('Ctrl Pts',(78.4538362502896,-2.44085980698392,339.269822767417));
#33192=CARTESIAN_POINT('Ctrl Pts',(78.446062579885,-2.32181928258195,339.337872718724));
#33193=CARTESIAN_POINT('Ctrl Pts',(78.4382889094803,-2.20005694586107,339.400868649127));
#33194=CARTESIAN_POINT('Ctrl Pts',(78.4305152390756,-2.07604791000877,339.458610561357));
#33195=CARTESIAN_POINT('Ctrl Pts',(78.4231034348987,-1.95781152461267,339.51366457368));
#33196=CARTESIAN_POINT('Ctrl Pts',(78.4156916307217,-1.83753316611684,339.563942597932));
#33197=CARTESIAN_POINT('Ctrl Pts',(78.4082798265448,-1.7156373622172,339.609313561027));
#33198=CARTESIAN_POINT('Ctrl Pts',(78.4005047477663,-1.5877670818572,339.656908290176));
#33199=CARTESIAN_POINT('Ctrl Pts',(78.3927296689879,-1.45771270176755,339.699253184353));
#33200=CARTESIAN_POINT('Ctrl Pts',(78.3849545902095,-1.32594449117312,339.736143396143));
#33201=CARTESIAN_POINT('Ctrl Pts',(78.3771890791605,-1.19433842975042,339.772988212178));
#33202=CARTESIAN_POINT('Ctrl Pts',(78.3694235681114,-1.06102310688679,339.804391597075));
#33203=CARTESIAN_POINT('Ctrl Pts',(78.3616580570624,-0.926488089097307,
339.830196981828));
#33204=CARTESIAN_POINT('Ctrl Pts',(78.3539002455402,-0.792086463169742,
339.855976780467));
#33205=CARTESIAN_POINT('Ctrl Pts',(78.346142434018,-0.656467930357041,339.87616955148));
#33206=CARTESIAN_POINT('Ctrl Pts',(78.3383846224959,-0.520136175659759,
339.890668811244));
#33207=CARTESIAN_POINT('Ctrl Pts',(78.3306326489728,-0.383907014931307,
339.905157159854));
#33208=CARTESIAN_POINT('Ctrl Pts',(78.3228806754498,-0.246966087754619,
339.913960484225));
#33209=CARTESIAN_POINT('Ctrl Pts',(78.3151287019268,-0.109825854096218,
339.917023626572));
#33210=CARTESIAN_POINT('Ctrl Pts',(78.3073800113692,0.0272563005918082,
339.920085471677));
#33211=CARTESIAN_POINT('Ctrl Pts',(78.2996313208116,0.164537203919587,339.917411961076));
#33212=CARTESIAN_POINT('Ctrl Pts',(78.291882630254,0.301500927360121,339.908999923946));
#33213=CARTESIAN_POINT('Ctrl Pts',(78.2841355518761,0.438436154354049,339.90058963701));
#33214=CARTESIAN_POINT('Ctrl Pts',(78.2763884734983,0.575053942829135,339.88644322234));
#33215=CARTESIAN_POINT('Ctrl Pts',(78.2686413951205,0.710840418914877,339.86660959615));
#33216=CARTESIAN_POINT('Ctrl Pts',(78.2608942518146,0.846628033022075,339.846775803735));
#33217=CARTESIAN_POINT('Ctrl Pts',(78.2531471085088,0.98158393407312,339.821254761223));
#33218=CARTESIAN_POINT('Ctrl Pts',(78.245399965203,1.11520180378499,339.790146970536));
#33219=CARTESIAN_POINT('Ctrl Pts',(78.2376510801749,1.24884971363066,339.759032186157));
#33220=CARTESIAN_POINT('Ctrl Pts',(78.2299021951468,1.38115861292424,339.722328242876));
#33221=CARTESIAN_POINT('Ctrl Pts',(78.2221533101188,1.51163515289127,339.680186131667));
#33222=CARTESIAN_POINT('Ctrl Pts',(78.214396200344,1.64225018200598,339.637999290385));
#33223=CARTESIAN_POINT('Ctrl Pts',(78.2066390905693,1.77102859416182,339.590362871134));
#33224=CARTESIAN_POINT('Ctrl Pts',(78.1988819807946,1.89749439459063,339.53747706165));
#33225=CARTESIAN_POINT('Ctrl Pts',(78.1911207258684,2.0240277742996,339.48456299168));
#33226=CARTESIAN_POINT('Ctrl Pts',(78.1833594709422,2.14824572606224,339.42639410773));
#33227=CARTESIAN_POINT('Ctrl Pts',(78.175598216016,2.26969575972321,339.363217186984));
#33228=CARTESIAN_POINT('Ctrl Pts',(78.1678245456114,2.39134007385748,339.299939203755));
#33229=CARTESIAN_POINT('Ctrl Pts',(78.1600508752067,2.51020728281326,339.231637369767));
#33230=CARTESIAN_POINT('Ctrl Pts',(78.1522772048021,2.62587209361402,339.158602987841));
#33231=CARTESIAN_POINT('Ctrl Pts',(78.144865400625,2.73615267964465,339.088968373964));
#33232=CARTESIAN_POINT('Ctrl Pts',(78.1374535964479,2.84352206422753,339.015032060152));
#33233=CARTESIAN_POINT('Ctrl Pts',(78.1300417922708,2.94764028891242,338.937080109635));
#33234=CARTESIAN_POINT('Ctrl Pts',(78.1222667134924,3.05686165794124,338.855307501815));
#33235=CARTESIAN_POINT('Ctrl Pts',(78.114491634714,3.16285027042858,338.768857250998));
#33236=CARTESIAN_POINT('Ctrl Pts',(78.1067165559355,3.2651793761515,338.678013961917));
#33237=CARTESIAN_POINT('Ctrl Pts',(78.0989510448865,3.36738255939524,338.587282461286));
#33238=CARTESIAN_POINT('Ctrl Pts',(78.0911855338376,3.46593490654975,338.492168935626));
#33239=CARTESIAN_POINT('Ctrl Pts',(78.0834200227886,3.56043982286565,338.393000343391));
#33240=CARTESIAN_POINT('Ctrl Pts',(78.0756622112664,3.65485103728194,338.293930077104));
#33241=CARTESIAN_POINT('Ctrl Pts',(78.0679043997442,3.74522253911589,338.190813026624));
#33242=CARTESIAN_POINT('Ctrl Pts',(78.060146588222,3.83119221115989,338.084015127013));
#33243=CARTESIAN_POINT('Ctrl Pts',(78.052394614699,3.91709718829931,337.97729759621));
#33244=CARTESIAN_POINT('Ctrl Pts',(78.044642641176,3.99860668493804,337.866905032992));
#33245=CARTESIAN_POINT('Ctrl Pts',(78.036890667653,4.0753969962245,337.753238526838));
#33246=CARTESIAN_POINT('Ctrl Pts',(78.0291419770954,4.15215478676859,337.639620158516));
#33247=CARTESIAN_POINT('Ctrl Pts',(78.0213932865377,4.22419714863462,337.522730928156));
#33248=CARTESIAN_POINT('Ctrl Pts',(78.0136445959801,4.29124221687945,337.403002975148));
#33249=CARTESIAN_POINT('Ctrl Pts',(78.0058975176023,4.35827333583785,337.283299932541));
#33250=CARTESIAN_POINT('Ctrl Pts',(77.9981504392245,4.42030903841195,337.160759682901));
#33251=CARTESIAN_POINT('Ctrl Pts',(77.9904033608466,4.47711237265312,337.035840825098));
#33252=CARTESIAN_POINT('Ctrl Pts',(77.9826562175408,4.53391618296091,336.910920920355));
#33253=CARTESIAN_POINT('Ctrl Pts',(77.9749090742351,4.58548737567217,336.783622723504));
#33254=CARTESIAN_POINT('Ctrl Pts',(77.9671619309293,4.63163646712052,336.654426395745));
#33255=CARTESIAN_POINT('Ctrl Pts',(77.9594130459012,4.67779593386437,336.52520102191));
#33256=CARTESIAN_POINT('Ctrl Pts',(77.9516641608731,4.71853074220597,336.394077036026));
#33257=CARTESIAN_POINT('Ctrl Pts',(77.943915275845,4.7537008843459,336.261551015484));
#33258=CARTESIAN_POINT('Ctrl Pts',(77.9361581660703,4.78890835643812,336.128884330454));
#33259=CARTESIAN_POINT('Ctrl Pts',(77.9284010562956,4.81853926333295,335.994813016472));
#33260=CARTESIAN_POINT('Ctrl Pts',(77.9206439465208,4.8425043590867,335.859845680763));
#33261=CARTESIAN_POINT('Ctrl Pts',(77.9128826915947,4.86648226102134,335.724806222825));
#33262=CARTESIAN_POINT('Ctrl Pts',(77.9051214366685,4.88478826685253,335.588870176279));
#33263=CARTESIAN_POINT('Ctrl Pts',(77.8973601817424,4.89738502839247,335.452551595044));
#33264=CARTESIAN_POINT('Ctrl Pts',(77.8895865113377,4.9100019406456,335.316014948506));
#33265=CARTESIAN_POINT('Ctrl Pts',(77.8818128409331,4.91689133865514,335.179094935046));
#33266=CARTESIAN_POINT('Ctrl Pts',(77.8740391705284,4.91806803474277,335.04230683327));
#33267=CARTESIAN_POINT('Ctrl Pts',(77.8666273663513,4.91918995534444,334.91188625054));
#33268=CARTESIAN_POINT('Ctrl Pts',(77.8592155621741,4.91511906654999,334.78158586255));
#33269=CARTESIAN_POINT('Ctrl Pts',(77.8518037579969,4.90591195400692,334.651846352838));
#33270=CARTESIAN_POINT('Ctrl Pts',(77.8440286792185,4.89625357345165,334.515747923284));
#33271=CARTESIAN_POINT('Ctrl Pts',(77.83625360044,4.88091223304646,334.379836646643));
#33272=CARTESIAN_POINT('Ctrl Pts',(77.8284785216616,4.8598963239511,334.244625402236));
#33273=CARTESIAN_POINT('Ctrl Pts',(77.8207130106126,4.83890627626982,334.109580543874));
#33274=CARTESIAN_POINT('Ctrl Pts',(77.8129474995636,4.81225561336198,333.975234386281));
#33275=CARTESIAN_POINT('Ctrl Pts',(77.8051819885145,4.78000466139165,333.842097370426));
#33276=CARTESIAN_POINT('Ctrl Pts',(77.7974241769924,4.74778568633409,333.70909236031));
#33277=CARTESIAN_POINT('Ctrl Pts',(77.7896663654701,4.70997756383745,333.577294483556));
#33278=CARTESIAN_POINT('Ctrl Pts',(77.7819085539479,4.66669205410366,333.44720628071));
#33279=CARTESIAN_POINT('Ctrl Pts',(77.7741565804249,4.62343911808864,333.317215973363));
#33280=CARTESIAN_POINT('Ctrl Pts',(77.7664046069019,4.57471712220228,333.188933148429));
#33281=CARTESIAN_POINT('Ctrl Pts',(77.7586526333789,4.52068817587236,333.062847068756));
#33282=CARTESIAN_POINT('Ctrl Pts',(77.7509039428213,4.46668211083326,332.936814386612));
#33283=CARTESIAN_POINT('Ctrl Pts',(77.7431552522636,4.4073737190965,332.812976957912));
#33284=CARTESIAN_POINT('Ctrl Pts',(77.735406561706,4.34297386260081,332.69180566432));
#33285=CARTESIAN_POINT('Ctrl Pts',(77.7276594833282,4.27858740503314,332.570659581427));
#33286=CARTESIAN_POINT('Ctrl Pts',(77.7199124049503,4.20911177309933,332.452178875221));
#33287=CARTESIAN_POINT('Ctrl Pts',(77.7121653265725,4.13480438407849,332.336810977812));
#33288=CARTESIAN_POINT('Ctrl Pts',(77.7044181832667,4.06049637229022,332.221442113508));
#33289=CARTESIAN_POINT('Ctrl Pts',(77.6966710399609,3.98135673430004,332.109186438649));
#33290=CARTESIAN_POINT('Ctrl Pts',(77.6889238966551,3.8976867074221,332.000463136868));
#33291=CARTESIAN_POINT('Ctrl Pts',(77.681175011627,3.81399786974586,331.891715391782));
#33292=CARTESIAN_POINT('Ctrl Pts',(77.6734261265989,3.72577685476512,331.786501909754));
#33293=CARTESIAN_POINT('Ctrl Pts',(77.6656772415708,3.63336547874652,331.685209152849));
#33294=CARTESIAN_POINT('Ctrl Pts',(77.6579201317961,3.5408560163385,331.583808882766));
#33295=CARTESIAN_POINT('Ctrl Pts',(77.6501630220213,3.44414757206624,331.486337940004));
#33296=CARTESIAN_POINT('Ctrl Pts',(77.6424059122466,3.34361954849576,331.393146609936));
#33297=CARTESIAN_POINT('Ctrl Pts',(77.6346446573204,3.24303780596375,331.2999054814));
#33298=CARTESIAN_POINT('Ctrl Pts',(77.6268834023942,3.13863271450823,331.210948775761));
#33299=CARTESIAN_POINT('Ctrl Pts',(77.6191221474681,3.03081634178963,331.126586083977));
#33300=CARTESIAN_POINT('Ctrl Pts',(77.6113484770634,2.92282749801196,331.04208843938));
#33301=CARTESIAN_POINT('Ctrl Pts',(77.6035748066587,2.81141678620896,330.962199721863));
#33302=CARTESIAN_POINT('Ctrl Pts',(77.5958011362541,2.69702553095154,330.887186322249));
#33303=CARTESIAN_POINT('Ctrl Pts',(77.588389332077,2.58795921614838,330.815664814435));
#33304=CARTESIAN_POINT('Ctrl Pts',(77.5809775279,2.47618384853801,330.748575095096));
#33305=CARTESIAN_POINT('Ctrl Pts',(77.573565723723,2.36210063005212,330.686108059303));
#33306=CARTESIAN_POINT('Ctrl Pts',(77.5657906449446,2.24242585319067,330.620579328006));
#33307=CARTESIAN_POINT('Ctrl Pts',(77.5580155661661,2.1198330815448,330.559930798069));
#33308=CARTESIAN_POINT('Ctrl Pts',(77.5502404873877,1.99475814721351,330.504432961614));
#33309=CARTESIAN_POINT('Ctrl Pts',(77.5424749763387,1.86983712555165,330.44900341878));
#33310=CARTESIAN_POINT('Ctrl Pts',(77.5347094652897,1.74244037256878,330.398712115132));
#33311=CARTESIAN_POINT('Ctrl Pts',(77.5269439542407,1.61302977491208,330.353784550008));
#33312=CARTESIAN_POINT('Ctrl Pts',(77.5191861427185,1.48374748823964,330.308901530695));
#33313=CARTESIAN_POINT('Ctrl Pts',(77.5114283311963,1.35245569738056,330.269371793832));
#33314=CARTESIAN_POINT('Ctrl Pts',(77.5036705196741,1.21963747925856,330.235373311403));
#33315=CARTESIAN_POINT('Ctrl Pts',(77.495918546151,1.08691921105769,330.201400413911));
#33316=CARTESIAN_POINT('Ctrl Pts',(77.488166572628,0.952677179135595,330.172950582252));
#33317=CARTESIAN_POINT('Ctrl Pts',(77.480414599105,0.817410541770264,330.150152263349));
#33318=CARTESIAN_POINT('Ctrl Pts',(77.4726659085474,0.682201189906165,330.127363599547));
#33319=CARTESIAN_POINT('Ctrl Pts',(77.4649172179898,0.545968480273064,330.110221752988));
#33320=CARTESIAN_POINT('Ctrl Pts',(77.4571685274321,0.409222496802693,330.098804226456));
#33321=CARTESIAN_POINT('Ctrl Pts',(77.4494214490543,0.272504964476309,330.087389075435));
#33322=CARTESIAN_POINT('Ctrl Pts',(77.4416743706765,0.135274760001691,330.081695907976));
#33323=CARTESIAN_POINT('Ctrl Pts',(77.4339272922987,-0.00195255815189377,
330.081750387585));
#33324=CARTESIAN_POINT('Ctrl Pts',(77.4261801489929,-0.139181026402485,
330.081804867652));
#33325=CARTESIAN_POINT('Ctrl Pts',(77.418433005687,-0.276406217409533,330.087607090712));
#33326=CARTESIAN_POINT('Ctrl Pts',(77.4106858623812,-0.413112613915317,
330.0991305842));
#33327=CARTESIAN_POINT('Ctrl Pts',(77.4029369773531,-0.549849744921395,
330.110656668414));
#33328=CARTESIAN_POINT('Ctrl Pts',(77.3951880923251,-0.686067459916694,
330.127906549751));
#33329=CARTESIAN_POINT('Ctrl Pts',(77.387439207297,-0.821255798311222,330.150801924417));
#33330=CARTESIAN_POINT('Ctrl Pts',(77.3796820975222,-0.956587627004879,
330.17372160047));
#33331=CARTESIAN_POINT('Ctrl Pts',(77.3719249877475,-1.09088751054967,330.202298674433));
#33332=CARTESIAN_POINT('Ctrl Pts',(77.3641678779728,-1.22365557000473,330.236403658107));
#33333=CARTESIAN_POINT('Ctrl Pts',(77.3564066230466,-1.35649457646567,330.270526866394));
#33334=CARTESIAN_POINT('Ctrl Pts',(77.3486453681204,-1.48779975379558,330.310183757427));
#33335=CARTESIAN_POINT('Ctrl Pts',(77.3408841131943,-1.61708776689569,330.355195352153));
#33336=CARTESIAN_POINT('Ctrl Pts',(77.3331104427896,-1.74658259868188,330.400278950762));
#33337=CARTESIAN_POINT('Ctrl Pts',(77.325336772385,-1.87405345449498,330.450734226098));
#33338=CARTESIAN_POINT('Ctrl Pts',(77.3175631019803,-1.99903749455962,330.506334218275));
#33339=CARTESIAN_POINT('Ctrl Pts',(77.3101512978032,-2.11820349749059,330.55934601744));
#33340=CARTESIAN_POINT('Ctrl Pts',(77.302739493626,-2.23510873886439,330.617034211946));
#33341=CARTESIAN_POINT('Ctrl Pts',(77.2953276894489,-2.34937557755609,330.679164726805));
#33342=CARTESIAN_POINT('Ctrl Pts',(77.2875526106704,-2.46924297439482,330.744340443275));
#33343=CARTESIAN_POINT('Ctrl Pts',(77.279777531892,-2.58658560020835,330.814610920793));
#33344=CARTESIAN_POINT('Ctrl Pts',(77.2720024531136,-2.70094013864279,330.889756037658));
#33345=CARTESIAN_POINT('Ctrl Pts',(77.2642369420646,-2.81515395653753,330.964808683673));
#33346=CARTESIAN_POINT('Ctrl Pts',(77.2564714310155,-2.92638667975617,331.044723821029));
#33347=CARTESIAN_POINT('Ctrl Pts',(77.2487059199665,-3.03419872772709,331.129235070021));
#33348=CARTESIAN_POINT('Ctrl Pts',(77.2409481084443,-3.14190387973842,331.213662525863));
#33349=CARTESIAN_POINT('Ctrl Pts',(77.2331902969222,-3.24619480035211,331.302676784951));
#33350=CARTESIAN_POINT('Ctrl Pts',(77.2254324854,-3.34666040848534,331.395967928448));
#33351=CARTESIAN_POINT('Ctrl Pts',(77.2176805118769,-3.44705041306257,331.489188867401));
#33352=CARTESIAN_POINT('Ctrl Pts',(77.2099285383539,-3.54362054973467,331.58668001961));
#33353=CARTESIAN_POINT('Ctrl Pts',(77.2021765648309,-3.63599268155756,331.688091142232));
#33354=CARTESIAN_POINT('Ctrl Pts',(77.1944278742732,-3.72832569372784,331.789459317184));
#33355=CARTESIAN_POINT('Ctrl Pts',(77.1866791837157,-3.8164639744186,331.89474387234));
#33356=CARTESIAN_POINT('Ctrl Pts',(77.178930493158,-3.9000663142004,332.003557808444));
#33357=CARTESIAN_POINT('Ctrl Pts',(77.1711834147802,-3.98365125981715,332.112349104899));
#33358=CARTESIAN_POINT('Ctrl Pts',(77.1634363364023,-4.06270190370081,332.224668011934));
#33359=CARTESIAN_POINT('Ctrl Pts',(77.1556892580245,-4.13691766658959,332.340094873429));
#33360=CARTESIAN_POINT('Ctrl Pts',(77.1479421147187,-4.21113405147789,332.455522702312));
#33361=CARTESIAN_POINT('Ctrl Pts',(77.1401949714129,-4.28051526315522,332.57405820883));
#33362=CARTESIAN_POINT('Ctrl Pts',(77.132447828107,-4.34480458699867,332.6952535577));
#33363=CARTESIAN_POINT('Ctrl Pts',(77.124698943079,-4.40910836444697,332.816476153857));
#33364=CARTESIAN_POINT('Ctrl Pts',(77.1169500580509,-4.46831779297572,332.940359437063));
#33365=CARTESIAN_POINT('Ctrl Pts',(77.1092011730228,-4.52222275097801,333.066432195904));
#33366=CARTESIAN_POINT('Ctrl Pts',(77.101444063248,-4.5761849242597,333.192638769674));
#33367=CARTESIAN_POINT('Ctrl Pts',(77.0936869534733,-4.62483122621104,333.321039101383));
#33368=CARTESIAN_POINT('Ctrl Pts',(77.0859298436986,-4.66800003304214,333.451142758671));
#33369=CARTESIAN_POINT('Ctrl Pts',(77.0781685887724,-4.71119190790331,333.581315939193));
#33370=CARTESIAN_POINT('Ctrl Pts',(77.0704073338462,-4.74890034793319,333.713193883333));
#33371=CARTESIAN_POINT('Ctrl Pts',(77.06264607892,-4.78101430008077,333.846273288459));
#33372=CARTESIAN_POINT('Ctrl Pts',(77.0548724085154,-4.81317962408587,333.979565577263));
#33373=CARTESIAN_POINT('Ctrl Pts',(77.0470987381107,-4.83973250099611,334.114062783995));
#33374=CARTESIAN_POINT('Ctrl Pts',(77.039325067706,-4.86061331706203,334.249252875797));
#33375=CARTESIAN_POINT('Ctrl Pts',(77.031913263529,-4.88052212611612,334.378149836299));
#33376=CARTESIAN_POINT('Ctrl Pts',(77.0245014593521,-4.89527502676103,334.507676340026));
#33377=CARTESIAN_POINT('Ctrl Pts',(77.0170896551751,-4.90486449436498,334.637388149094));
#33378=CARTESIAN_POINT('Ctrl Pts',(77.0102385196134,-4.91372856321389,334.757287861317));
#33379=CARTESIAN_POINT('Ctrl Pts',(77.0033873840517,-4.91819683629662,334.877516539856));
#33380=CARTESIAN_POINT('Ctrl Pts',(76.99653624849,-4.91824952845158,334.997846308785));
#33381=CARTESIAN_POINT('',(80.4965362485215,-4.91824999789874,334.999856232645));
#33382=CARTESIAN_POINT('Ctrl Pts',(80.49653624849,-4.91824999789876,334.999856233204));
#33383=CARTESIAN_POINT('Ctrl Pts',(80.4884388234102,-4.91825420074369,335.143635204458));
#33384=CARTESIAN_POINT('Ctrl Pts',(80.4803413983304,-4.91194928860781,335.287298548783));
#33385=CARTESIAN_POINT('Ctrl Pts',(80.4722439732506,-4.89939146504502,335.430286340411));
#33386=CARTESIAN_POINT('Ctrl Pts',(80.4641365277192,-4.88681810134926,335.573451077453));
#33387=CARTESIAN_POINT('Ctrl Pts',(80.4560290821879,-4.86797641677283,335.715938259107));
#33388=CARTESIAN_POINT('Ctrl Pts',(80.4479216366565,-4.84297405980445,335.857196196073));
#33389=CARTESIAN_POINT('Ctrl Pts',(80.4397956744712,-4.81791459977065,335.99877675307));
#33390=CARTESIAN_POINT('Ctrl Pts',(80.4316697122859,-4.7866663951556,336.139122120127));
#33391=CARTESIAN_POINT('Ctrl Pts',(80.4235437501005,-4.74938795704269,336.277692097494));
#33392=CARTESIAN_POINT('Ctrl Pts',(80.4154080949667,-4.71206505182863,336.416427366259));
#33393=CARTESIAN_POINT('Ctrl Pts',(80.4072724398328,-4.6686976604577,336.553382698982));
#33394=CARTESIAN_POINT('Ctrl Pts',(80.3991367846989,-4.61949320795949,336.688036007944));
#33395=CARTESIAN_POINT('Ctrl Pts',(80.3909826162357,-4.57017678682203,336.822995731204));
#33396=CARTESIAN_POINT('Ctrl Pts',(80.3828284477725,-4.51499687380978,336.955642644701));
#33397=CARTESIAN_POINT('Ctrl Pts',(80.3746742793093,-4.45420855474063,337.085475776262));
#33398=CARTESIAN_POINT('Ctrl Pts',(80.3684315416936,-4.4076697166291,337.184874528913));
#33399=CARTESIAN_POINT('Ctrl Pts',(80.362188804078,-4.35784461194631,337.282624521531));
#33400=CARTESIAN_POINT('Ctrl Pts',(80.3559460664624,-4.30486496663268,337.378512283247));
#33401=CARTESIAN_POINT('Ctrl Pts',(80.3481709876839,-4.23888094786888,337.497936636333));
#33402=CARTESIAN_POINT('Ctrl Pts',(80.3403959089054,-4.16781934094549,337.614801857271));
#33403=CARTESIAN_POINT('Ctrl Pts',(80.332620830127,-4.09190339257262,337.728646127359));
#33404=CARTESIAN_POINT('Ctrl Pts',(80.324855319078,-4.01608086360727,337.842350304825));
#33405=CARTESIAN_POINT('Ctrl Pts',(80.317089808029,-3.9354160936803,337.953040606053));
#33406=CARTESIAN_POINT('Ctrl Pts',(80.30932429698,-3.8501784260975,338.060279260086));
#33407=CARTESIAN_POINT('Ctrl Pts',(80.3015664854578,-3.76502527191038,338.167411586682));
#33408=CARTESIAN_POINT('Ctrl Pts',(80.2938086739356,-3.67530848471277,338.271098772671));
#33409=CARTESIAN_POINT('Ctrl Pts',(80.2860508624134,-3.58134075341484,338.370931840075));
#33410=CARTESIAN_POINT('Ctrl Pts',(80.2782988888904,-3.4874437358146,338.470689779929));
#33411=CARTESIAN_POINT('Ctrl Pts',(80.2705469153674,-3.38930240833154,338.566599090717));
#33412=CARTESIAN_POINT('Ctrl Pts',(80.2627949418444,-3.2872695604019,338.658284010264));
#33413=CARTESIAN_POINT('Ctrl Pts',(80.2550462512868,-3.18527992344387,338.749930101193));
#33414=CARTESIAN_POINT('Ctrl Pts',(80.2472975607291,-3.07940233405125,338.83735509843));
#33415=CARTESIAN_POINT('Ctrl Pts',(80.2395488701715,-2.97002608776162,338.920220414787));
#33416=CARTESIAN_POINT('Ctrl Pts',(80.2318017917937,-2.86067259811348,339.003068490323));
#33417=CARTESIAN_POINT('Ctrl Pts',(80.2240547134158,-2.74782221082323,339.081358536079));
#33418=CARTESIAN_POINT('Ctrl Pts',(80.216307635038,-2.63189660306024,339.154792814726));
#33419=CARTESIAN_POINT('Ctrl Pts',(80.2085604917322,-2.51597002372916,339.228227708824));
#33420=CARTESIAN_POINT('Ctrl Pts',(80.2008133484263,-2.39696850271764,339.296806545474));
#33421=CARTESIAN_POINT('Ctrl Pts',(80.1930662051205,-2.27534159938073,339.360275641359));
#33422=CARTESIAN_POINT('Ctrl Pts',(80.1853173200924,-2.1536873517334,339.423759006444));
#33423=CARTESIAN_POINT('Ctrl Pts',(80.1775684350643,-2.02940689370761,339.482130164028));
#33424=CARTESIAN_POINT('Ctrl Pts',(80.1698195500362,-1.90297284548634,339.535182180667));
#33425=CARTESIAN_POINT('Ctrl Pts',(80.1620624402614,-1.77640459886032,339.588290507265));
#33426=CARTESIAN_POINT('Ctrl Pts',(80.1543053304867,-1.64767855685277,339.636068263444));
#33427=CARTESIAN_POINT('Ctrl Pts',(80.146548220712,-1.51728623251546,339.678357142322));
#33428=CARTESIAN_POINT('Ctrl Pts',(80.1387869657858,-1.38682423068908,339.720668619026));
#33429=CARTESIAN_POINT('Ctrl Pts',(80.1310257108596,-1.2546945486543,339.757485269138));
#33430=CARTESIAN_POINT('Ctrl Pts',(80.1232644559335,-1.12140122780007,339.788699442311));
#33431=CARTESIAN_POINT('Ctrl Pts',(80.1154907855288,-0.987894681072749,
339.819963547988));
#33432=CARTESIAN_POINT('Ctrl Pts',(80.1077171151241,-0.85322115998913,339.845607194568));
#33433=CARTESIAN_POINT('Ctrl Pts',(80.0999434447194,-0.717893088456906,
339.865574228809));
#33434=CARTESIAN_POINT('Ctrl Pts',(80.0925316405424,-0.588864571213662,
339.884611792801));
#33435=CARTESIAN_POINT('Ctrl Pts',(80.0851198363654,-0.459241356943298,
339.89848931303));
#33436=CARTESIAN_POINT('Ctrl Pts',(80.0777080321884,-0.329467724227514,
339.907202266179));
#33437=CARTESIAN_POINT('Ctrl Pts',(80.0699329534099,-0.193333499195371,
339.916342267116));
#33438=CARTESIAN_POINT('Ctrl Pts',(80.0621578746315,-0.0566035286780677,
339.919827522596));
#33439=CARTESIAN_POINT('Ctrl Pts',(80.0543827958531,0.0802130225205787,
339.917595848941));
#33440=CARTESIAN_POINT('Ctrl Pts',(80.0466172848041,0.216861212242528,339.915366921502));
#33441=CARTESIAN_POINT('Ctrl Pts',(80.038851773755,0.353595383569523,339.907435068965));
#33442=CARTESIAN_POINT('Ctrl Pts',(80.031086262706,0.489901648447737,339.893789884879));
#33443=CARTESIAN_POINT('Ctrl Pts',(80.0233284511838,0.626072765267665,339.880158230033));
#33444=CARTESIAN_POINT('Ctrl Pts',(80.0155706396617,0.761816433536126,339.860824555563));
#33445=CARTESIAN_POINT('Ctrl Pts',(80.0078128281395,0.896619521033607,339.835830486793));
#33446=CARTESIAN_POINT('Ctrl Pts',(80.0000608546165,1.0313211649328,339.810855226853));
#33447=CARTESIAN_POINT('Ctrl Pts',(79.9923088810934,1.16508325415929,339.780228122162));
#33448=CARTESIAN_POINT('Ctrl Pts',(79.9845569075704,1.29739888767643,339.744042494409));
#33449=CARTESIAN_POINT('Ctrl Pts',(79.9768082170128,1.42965848544431,339.707872191291));
#33450=CARTESIAN_POINT('Ctrl Pts',(79.9690595264552,1.56047246962644,339.666148150021));
#33451=CARTESIAN_POINT('Ctrl Pts',(79.9613108358975,1.68934544488028,339.619014508568));
#33452=CARTESIAN_POINT('Ctrl Pts',(79.9535637575197,1.81819160703517,339.571890673663));
#33453=CARTESIAN_POINT('Ctrl Pts',(79.9458166791419,1.94509719667202,339.519359611473));
#33454=CARTESIAN_POINT('Ctrl Pts',(79.9380696007641,2.06958364640867,339.461614796575));
#33455=CARTESIAN_POINT('Ctrl Pts',(79.9303224574582,2.19407113946175,339.40386949772));
#33456=CARTESIAN_POINT('Ctrl Pts',(79.9225753141524,2.31613909759164,339.34091052348));
#33457=CARTESIAN_POINT('Ctrl Pts',(79.9148281708466,2.43533091072103,339.272978635307));
#33458=CARTESIAN_POINT('Ctrl Pts',(79.9070792858185,2.55454952070028,339.205031474603));
#33459=CARTESIAN_POINT('Ctrl Pts',(79.8993304007905,2.67089035945508,339.132109368747));
#33460=CARTESIAN_POINT('Ctrl Pts',(79.8915815157624,2.78392365033828,339.054497770574));
#33461=CARTESIAN_POINT('Ctrl Pts',(79.8838244059876,2.89707691592442,338.976803794648));
#33462=CARTESIAN_POINT('Ctrl Pts',(79.8760672962129,3.00691529801813,338.89441060503));
#33463=CARTESIAN_POINT('Ctrl Pts',(79.8683101864382,3.11303968706979,338.807645856593));
#33464=CARTESIAN_POINT('Ctrl Pts',(79.860548931512,3.21922078560176,338.720834743849));
#33465=CARTESIAN_POINT('Ctrl Pts',(79.8527876765858,3.32168364467873,338.629647677277));
#33466=CARTESIAN_POINT('Ctrl Pts',(79.8450264216596,3.42006497310803,338.534450260255));
#33467=CARTESIAN_POINT('Ctrl Pts',(79.837252751255,3.51860367960042,338.439100558391));
#33468=CARTESIAN_POINT('Ctrl Pts',(79.8294790808503,3.61304753891622,338.339727969975));
#33469=CARTESIAN_POINT('Ctrl Pts',(79.8217054104457,3.70307202861645,338.236733015461));
#33470=CARTESIAN_POINT('Ctrl Pts',(79.8142936062686,3.78890585666236,338.13853250086));
#33471=CARTESIAN_POINT('Ctrl Pts',(79.8068818020915,3.87072231850769,338.037039497077));
#33472=CARTESIAN_POINT('Ctrl Pts',(79.7994699979144,3.94827718576553,337.932625159625));
#33473=CARTESIAN_POINT('Ctrl Pts',(79.791694919136,4.02963324809187,337.823093164459));
#33474=CARTESIAN_POINT('Ctrl Pts',(79.7839198403575,4.10655650639041,337.710000086969));
#33475=CARTESIAN_POINT('Ctrl Pts',(79.7761447615791,4.17871913078881,337.593740443545));
#33476=CARTESIAN_POINT('Ctrl Pts',(79.7683792505301,4.25079295448369,337.477623865013));
#33477=CARTESIAN_POINT('Ctrl Pts',(79.7606137394811,4.3181175963772,337.358348802712));
#33478=CARTESIAN_POINT('Ctrl Pts',(79.7528482284321,4.38040621114947,337.236341764539));
#33479=CARTESIAN_POINT('Ctrl Pts',(79.7450904169099,4.44263306657881,337.114455696701));
#33480=CARTESIAN_POINT('Ctrl Pts',(79.7373326053877,4.49983365512129,336.989843389468));
#33481=CARTESIAN_POINT('Ctrl Pts',(79.7295747938655,4.55176529511207,336.862958872523));
#33482=CARTESIAN_POINT('Ctrl Pts',(79.7218228203425,4.60365785489695,336.736169840201));
#33483=CARTESIAN_POINT('Ctrl Pts',(79.7140708468195,4.65028921090893,336.60711236195));
#33484=CARTESIAN_POINT('Ctrl Pts',(79.7063188732965,4.69146352611045,336.476263203387));
#33485=CARTESIAN_POINT('Ctrl Pts',(79.6985701827389,4.73262040396502,336.345469459521));
#33486=CARTESIAN_POINT('Ctrl Pts',(79.6908214921813,4.76832472046394,336.212885916572));
#33487=CARTESIAN_POINT('Ctrl Pts',(79.6830728016237,4.79842959745354,336.079007164379));
#33488=CARTESIAN_POINT('Ctrl Pts',(79.6753257232458,4.82852821087205,335.945156266779));
#33489=CARTESIAN_POINT('Ctrl Pts',(79.667578644868,4.85302961636937,335.810011077058));
#33490=CARTESIAN_POINT('Ctrl Pts',(79.6598315664902,4.87183753057354,335.674078732935));
#33491=CARTESIAN_POINT('Ctrl Pts',(79.6520844231844,4.89064560240612,335.538145249568));
#33492=CARTESIAN_POINT('Ctrl Pts',(79.6443372798786,4.90376003419864,335.401424985824));
#33493=CARTESIAN_POINT('Ctrl Pts',(79.6365901365728,4.91113618947991,335.264432204697));
#33494=CARTESIAN_POINT('Ctrl Pts',(79.6288412515447,4.91851400307749,335.127408624684));
#33495=CARTESIAN_POINT('Ctrl Pts',(79.6210923665166,4.92015095202456,334.990112795603));
#33496=CARTESIAN_POINT('Ctrl Pts',(79.6133434814885,4.91605450289538,334.853060600716));
#33497=CARTESIAN_POINT('Ctrl Pts',(79.6055863717138,4.91195370575279,334.715862937213));
#33498=CARTESIAN_POINT('Ctrl Pts',(79.5978292619391,4.90210736589721,334.578909815789));
#33499=CARTESIAN_POINT('Ctrl Pts',(79.5900721521644,4.88657503422405,334.442714169031));
#33500=CARTESIAN_POINT('Ctrl Pts',(79.5823108972382,4.87103440256944,334.306445743675));
#33501=CARTESIAN_POINT('Ctrl Pts',(79.574549642312,4.84980178526318,334.170935985494));
#33502=CARTESIAN_POINT('Ctrl Pts',(79.5667883873859,4.82298802827421,334.036688242767));
#33503=CARTESIAN_POINT('Ctrl Pts',(79.5590147169812,4.79613137801264,333.902225747403));
#33504=CARTESIAN_POINT('Ctrl Pts',(79.5512410465765,4.7636758398557,333.769029681643));
#33505=CARTESIAN_POINT('Ctrl Pts',(79.5434673761719,4.72578260228544,333.637589687929));
#33506=CARTESIAN_POINT('Ctrl Pts',(79.5360555719948,4.68965330404046,333.512268257545));
#33507=CARTESIAN_POINT('Ctrl Pts',(79.5286437678177,4.64858125403317,333.388543361287));
#33508=CARTESIAN_POINT('Ctrl Pts',(79.5212319636405,4.60274639885732,333.266821229559));
#33509=CARTESIAN_POINT('Ctrl Pts',(79.5134568848621,4.55466504089446,333.139133133565));
#33510=CARTESIAN_POINT('Ctrl Pts',(79.5056818060836,4.50119024821905,333.013245571066));
#33511=CARTESIAN_POINT('Ctrl Pts',(79.4979067273052,4.44247637052532,332.889647716654));
#33512=CARTESIAN_POINT('Ctrl Pts',(79.4901412162561,4.38383474399608,332.76620195727));
#33513=CARTESIAN_POINT('Ctrl Pts',(79.4823757052071,4.31996702630035,332.64504064938));
#33514=CARTESIAN_POINT('Ctrl Pts',(79.4746101941581,4.25107664856845,332.526635815231));
#33515=CARTESIAN_POINT('Ctrl Pts',(79.4668523826359,4.18225457584668,332.40834837982));
#33516=CARTESIAN_POINT('Ctrl Pts',(79.4590945711137,4.10841994883713,332.292812314898));
#33517=CARTESIAN_POINT('Ctrl Pts',(79.4513367595915,4.02982324181151,332.180477398165));
#33518=CARTESIAN_POINT('Ctrl Pts',(79.4435847860686,3.95128568130079,332.068227017021));
#33519=CARTESIAN_POINT('Ctrl Pts',(79.4358328125456,3.86799339696418,331.959173308117));
#33520=CARTESIAN_POINT('Ctrl Pts',(79.4280808390226,3.78024133252202,331.853738960227));
#33521=CARTESIAN_POINT('Ctrl Pts',(79.420332148465,3.69252643113077,331.748349263846));
#33522=CARTESIAN_POINT('Ctrl Pts',(79.4125834579074,3.60035575569038,331.646576179652));
#33523=CARTESIAN_POINT('Ctrl Pts',(79.4048347673498,3.50406573314971,331.54881087156));
#33524=CARTESIAN_POINT('Ctrl Pts',(79.3970876889719,3.40779574455252,331.451065904356));
#33525=CARTESIAN_POINT('Ctrl Pts',(79.3893406105941,3.30740838772562,331.357327332971));
#33526=CARTESIAN_POINT('Ctrl Pts',(79.3815935322163,3.20327802113654,331.267950565466));
#33527=CARTESIAN_POINT('Ctrl Pts',(79.3738463889105,3.09914678183477,331.178573048898));
#33528=CARTESIAN_POINT('Ctrl Pts',(79.3660992456047,2.99127276680282,331.093557663701));
#33529=CARTESIAN_POINT('Ctrl Pts',(79.3583521022989,2.88006427540641,331.013220242849));
#33530=CARTESIAN_POINT('Ctrl Pts',(79.3506032172708,2.7688307819798,330.93286476044));
#33531=CARTESIAN_POINT('Ctrl Pts',(79.3428543322426,2.65426163723137,330.857189563999));
#33532=CARTESIAN_POINT('Ctrl Pts',(79.3351054472145,2.53679469899179,330.786467548758));
#33533=CARTESIAN_POINT('Ctrl Pts',(79.3273483374398,2.41920308013039,330.71567046844));
#33534=CARTESIAN_POINT('Ctrl Pts',(79.319591227665,2.29870785907907,330.649837273316));
#33535=CARTESIAN_POINT('Ctrl Pts',(79.3118341178903,2.17577259820048,330.589195463023));
#33536=CARTESIAN_POINT('Ctrl Pts',(79.3040728629641,2.0527716446491,330.528521247685));
#33537=CARTESIAN_POINT('Ctrl Pts',(79.2963116080379,1.92732841046835,330.473044102855));
#33538=CARTESIAN_POINT('Ctrl Pts',(79.2885503531117,1.79992615707916,330.42294320643));
#33539=CARTESIAN_POINT('Ctrl Pts',(79.280776682707,1.67232010160502,330.372762164899));
#33540=CARTESIAN_POINT('Ctrl Pts',(79.2730030123024,1.54274913429885,330.327974685372));
#33541=CARTESIAN_POINT('Ctrl Pts',(79.2652293418977,1.41171223427289,330.288710194638));
#33542=CARTESIAN_POINT('Ctrl Pts',(79.2578175377207,1.2867751334696,330.251273475395));
#33543=CARTESIAN_POINT('Ctrl Pts',(79.2504057335436,1.16050578567972,330.218857197782));
#33544=CARTESIAN_POINT('Ctrl Pts',(79.2429939293666,1.03334317814458,330.191529875451));
#33545=CARTESIAN_POINT('Ctrl Pts',(79.2352188505882,0.899947952415436,330.162863159649));
#33546=CARTESIAN_POINT('Ctrl Pts',(79.2274437718097,0.765148136717748,330.139706270149));
#33547=CARTESIAN_POINT('Ctrl Pts',(79.2196686930313,0.629438615876122,330.122194131441));
#33548=CARTESIAN_POINT('Ctrl Pts',(79.2119031819823,0.493896094239676,330.104703542535));
#33549=CARTESIAN_POINT('Ctrl Pts',(79.2041376709332,0.357446478798141,330.09284393297));
#33550=CARTESIAN_POINT('Ctrl Pts',(79.1963721598842,0.220596791386352,330.086699671491));
#33551=CARTESIAN_POINT('Ctrl Pts',(79.188614348362,0.0838827908378721,330.080561502064));
#33552=CARTESIAN_POINT('Ctrl Pts',(79.1808565368398,-0.0532301043145716,
330.080127420922));
#33553=CARTESIAN_POINT('Ctrl Pts',(79.1730987253176,-0.190228120404908,
330.085430199427));
#33554=CARTESIAN_POINT('Ctrl Pts',(79.1653467517946,-0.327123041143866,
330.090728987423));
#33555=CARTESIAN_POINT('Ctrl Pts',(79.1575947782716,-0.463902865886357,
330.101756026896));
#33556=CARTESIAN_POINT('Ctrl Pts',(79.1498428047485,-0.600052535652913,
330.118492034529));
#33557=CARTESIAN_POINT('Ctrl Pts',(79.1420941141909,-0.736144545953213,
330.135220954453));
#33558=CARTESIAN_POINT('Ctrl Pts',(79.1343454236333,-0.871606544918365,
330.157653986211));
#33559=CARTESIAN_POINT('Ctrl Pts',(79.1265967330757,-1.00592753454227,330.185719902441));
#33560=CARTESIAN_POINT('Ctrl Pts',(79.1188496546978,-1.14022057756231,330.213779979324));
#33561=CARTESIAN_POINT('Ctrl Pts',(79.11110257632,-1.27337270106844,330.247470529656));
#33562=CARTESIAN_POINT('Ctrl Pts',(79.1033554979422,-1.40488244799375,330.28666907911));
#33563=CARTESIAN_POINT('Ctrl Pts',(79.0956083546363,-1.53639329709758,330.325867957086));
#33564=CARTESIAN_POINT('Ctrl Pts',(79.0878612113306,-1.66626136757738,330.370574814605));
#33565=CARTESIAN_POINT('Ctrl Pts',(79.0801140680247,-1.79400011453196,330.420617219367));
#33566=CARTESIAN_POINT('Ctrl Pts',(79.0723651829967,-1.92176757986786,330.470670874723));
#33567=CARTESIAN_POINT('Ctrl Pts',(79.0646162979686,-2.04740440521303,330.526062321731));
#33568=CARTESIAN_POINT('Ctrl Pts',(79.0568674129405,-2.17044415714877,330.586571035669));
#33569=CARTESIAN_POINT('Ctrl Pts',(79.0491103031658,-2.29361450474921,330.647143974181));
#33570=CARTESIAN_POINT('Ctrl Pts',(79.0413531933911,-2.41418192114389,330.712844856826));
#33571=CARTESIAN_POINT('Ctrl Pts',(79.0335960836164,-2.53170423684092,330.783406977231));
#33572=CARTESIAN_POINT('Ctrl Pts',(79.0258348286902,-2.64928935270599,330.854006803778));
#33573=CARTESIAN_POINT('Ctrl Pts',(79.018073573764,-2.76382579929253,330.929472829269));
#33574=CARTESIAN_POINT('Ctrl Pts',(79.0103123188378,-2.87490138160072,331.009495632308));
#33575=CARTESIAN_POINT('Ctrl Pts',(79.0025386484332,-2.98615464864084,331.089646445752));
#33576=CARTESIAN_POINT('Ctrl Pts',(78.9947649780285,-3.09393568086345,331.174368361358));
#33577=CARTESIAN_POINT('Ctrl Pts',(78.9869913076239,-3.19786561429249,331.263311817207));
#33578=CARTESIAN_POINT('Ctrl Pts',(78.9795795034468,-3.29695758431673,331.348114933788));
#33579=CARTESIAN_POINT('Ctrl Pts',(78.9721676992696,-3.39254871315622,331.436755214322));
#33580=CARTESIAN_POINT('Ctrl Pts',(78.9647558950925,-3.48434382503395,331.52890058174));
#33581=CARTESIAN_POINT('Ctrl Pts',(78.9570876850303,-3.57931452093268,331.62423365001));
#33582=CARTESIAN_POINT('Ctrl Pts',(78.9494194749681,-3.67054001882114,331.723638429202));
#33583=CARTESIAN_POINT('Ctrl Pts',(78.9417512649058,-3.75764359407961,331.826784330939));
#33584=CARTESIAN_POINT('Ctrl Pts',(78.9340926753545,-3.84463788948101,331.92980082617));
#33585=CARTESIAN_POINT('Ctrl Pts',(78.9264340858032,-3.92752028986851,332.036548804794));
#33586=CARTESIAN_POINT('Ctrl Pts',(78.9187754962519,-4.00594956814597,332.146659655777));
#33587=CARTESIAN_POINT('Ctrl Pts',(78.9111257385923,-4.084288401716,332.256643526837));
#33588=CARTESIAN_POINT('Ctrl Pts',(78.9034759809327,-4.15818410357815,332.369982224781));
#33589=CARTESIAN_POINT('Ctrl Pts',(78.8958262232731,-4.2273350211452,332.486273347896));
#33590=CARTESIAN_POINT('Ctrl Pts',(78.8881814101921,-4.29644124159077,332.602489303845));
#33591=CARTESIAN_POINT('Ctrl Pts',(78.8805365971111,-4.3608085705587,332.721653546066));
#33592=CARTESIAN_POINT('Ctrl Pts',(78.8728917840301,-4.42017816297547,332.84333403837));
#33593=CARTESIAN_POINT('Ctrl Pts',(78.8652501499995,-4.47952306689786,332.964963930559));
#33594=CARTESIAN_POINT('Ctrl Pts',(78.8576085159689,-4.53387419159026,333.089107630533));
#33595=CARTESIAN_POINT('Ctrl Pts',(78.8499668819382,-4.58301850033601,333.215308293268));
#33596=CARTESIAN_POINT('Ctrl Pts',(78.8423266643605,-4.63215369969497,333.341485563454));
#33597=CARTESIAN_POINT('Ctrl Pts',(78.8346864467829,-4.67608385838579,333.469718662477));
#33598=CARTESIAN_POINT('Ctrl Pts',(78.8270462292052,-4.71464418982511,333.599531069303));
#33599=CARTESIAN_POINT('Ctrl Pts',(78.8194030799807,-4.75321931734449,333.729393286768));
#33600=CARTESIAN_POINT('Ctrl Pts',(78.8117599307562,-4.78642038397138,333.860835637203));
#33601=CARTESIAN_POINT('Ctrl Pts',(78.8041167815318,-4.81413259656113,333.993366797077));
#33602=CARTESIAN_POINT('Ctrl Pts',(78.7964720323509,-4.84185061020636,334.125925699976));
#33603=CARTESIAN_POINT('Ctrl Pts',(78.78882728317,-4.86407741058527,334.259573469868));
#33604=CARTESIAN_POINT('Ctrl Pts',(78.7811825339891,-4.88074962362938,334.393810117256));
#33605=CARTESIAN_POINT('Ctrl Pts',(78.7735309956044,-4.8974366430522,334.52816597849));
#33606=CARTESIAN_POINT('Ctrl Pts',(78.7658794572198,-4.90855918837742,334.663111360645));
#33607=CARTESIAN_POINT('Ctrl Pts',(78.7582279188351,-4.91410588493564,334.798142589581));
#33608=CARTESIAN_POINT('Ctrl Pts',(78.7543306953963,-4.91693103129809,334.86691919945));
#33609=CARTESIAN_POINT('Ctrl Pts',(78.7504334719575,-4.91831049593728,334.935718080277));
#33610=CARTESIAN_POINT('Ctrl Pts',(78.7465362485187,-4.9182479660083,335.004472958214));
#33611=CARTESIAN_POINT('',(82.2465362484434,-4.91824801864532,334.995585298267));
#33612=CARTESIAN_POINT('Ctrl Pts',(82.2465362484433,-4.91824801864532,334.995585298267));
#33613=CARTESIAN_POINT('Ctrl Pts',(82.2388865763238,-4.9183691106983,335.130489259084));
#33614=CARTESIAN_POINT('Ctrl Pts',(82.2312369042042,-4.91293555636551,335.265570211825));
#33615=CARTESIAN_POINT('Ctrl Pts',(82.2235872320846,-4.90193044563438,335.40032607792));
#33616=CARTESIAN_POINT('Ctrl Pts',(82.215943816417,-4.89093433567417,335.534971730977));
#33617=CARTESIAN_POINT('Ctrl Pts',(82.2083004007494,-4.87437576652904,335.669292426584));
#33618=CARTESIAN_POINT('Ctrl Pts',(82.2006569850817,-4.85228989249124,335.802786311373));
#33619=CARTESIAN_POINT('Ctrl Pts',(82.1930173215805,-4.83021486044863,335.936214663774));
#33620=CARTESIAN_POINT('Ctrl Pts',(82.1853776580793,-4.80261798400293,336.068816615716));
#33621=CARTESIAN_POINT('Ctrl Pts',(82.1777379945781,-4.76958619491484,336.200096076061));
#33622=CARTESIAN_POINT('Ctrl Pts',(82.1701001475853,-4.73656225990584,336.33134432165));
#33623=CARTESIAN_POINT('Ctrl Pts',(82.1624623005925,-4.69810607956381,336.461270310194));
#33624=CARTESIAN_POINT('Ctrl Pts',(82.1548244535996,-4.65435545743641,336.589389297287));
#33625=CARTESIAN_POINT('Ctrl Pts',(82.1471866594079,-4.61060513776078,336.717507398683));
#33626=CARTESIAN_POINT('Ctrl Pts',(82.1395488652162,-4.56156057953586,336.843818142103));
#33627=CARTESIAN_POINT('Ctrl Pts',(82.1319110710244,-4.50740892574639,336.967853612086));
#33628=CARTESIAN_POINT('Ctrl Pts',(82.1242715661789,-4.45324514349038,337.091916862571));
#33629=CARTESIAN_POINT('Ctrl Pts',(82.1166320613334,-4.39397215282391,337.213703457217));
#33630=CARTESIAN_POINT('Ctrl Pts',(82.1089925564879,-4.32982429850132,337.33276758521));
#33631=CARTESIAN_POINT('Ctrl Pts',(82.1013451751211,-4.26561030613049,337.451954471308));
#33632=CARTESIAN_POINT('Ctrl Pts',(82.0936977937542,-4.19651160650226,337.568412931346));
#33633=CARTESIAN_POINT('Ctrl Pts',(82.0860504123874,-4.12280752497341,337.681723545506));
#33634=CARTESIAN_POINT('Ctrl Pts',(82.0783987493311,-4.04906217729369,337.795097601104));
#33635=CARTESIAN_POINT('Ctrl Pts',(82.0707470862748,-3.97070654760736,337.905319974378));
#33636=CARTESIAN_POINT('Ctrl Pts',(82.0630954232185,-3.88806115917067,338.012003234568));
#33637=CARTESIAN_POINT('Ctrl Pts',(82.0554323310357,-3.8052923250742,338.118845845275));
#33638=CARTESIAN_POINT('Ctrl Pts',(82.0477692388529,-3.71822119765673,338.222138480551));
#33639=CARTESIAN_POINT('Ctrl Pts',(82.0401061466702,-3.6272064637596,338.321529215852));
#33640=CARTESIAN_POINT('Ctrl Pts',(82.0351955218154,-3.56888285185939,338.385220295571));
#33641=CARTESIAN_POINT('Ctrl Pts',(82.0302848969607,-3.5089405527216,338.447309850742));
#33642=CARTESIAN_POINT('Ctrl Pts',(82.0253742721059,-3.44748098414941,338.507714059958));
#33643=CARTESIAN_POINT('Ctrl Pts',(82.0175991933275,-3.3501709673038,338.603353107756));
#33644=CARTESIAN_POINT('Ctrl Pts',(82.0098241145491,-3.24872437901894,338.695090894784));
#33645=CARTESIAN_POINT('Ctrl Pts',(82.0020490357706,-3.14348693104863,338.782548476467));
#33646=CARTESIAN_POINT('Ctrl Pts',(81.9942835247216,-3.03837898445794,338.869898436029));
#33647=CARTESIAN_POINT('Ctrl Pts',(81.9865180136726,-2.92948975772514,338.952978422756));
#33648=CARTESIAN_POINT('Ctrl Pts',(81.9787525026236,-2.81720228379485,339.031445690404));
#33649=CARTESIAN_POINT('Ctrl Pts',(81.9709946911015,-2.70502614322196,339.109835157528));
#33650=CARTESIAN_POINT('Ctrl Pts',(81.9632368795792,-2.58945877902461,339.183620784692));
#33651=CARTESIAN_POINT('Ctrl Pts',(81.955479068057,-2.47091655500107,339.252499787269));
#33652=CARTESIAN_POINT('Ctrl Pts',(81.947727094534,-2.35246353776014,339.321326956212));
#33653=CARTESIAN_POINT('Ctrl Pts',(81.939975121011,-2.23104045327232,339.385254654509));
#33654=CARTESIAN_POINT('Ctrl Pts',(81.932223147488,-2.10709262426579,339.444023372493));
#33655=CARTESIAN_POINT('Ctrl Pts',(81.9244744569304,-1.98319728723834,339.50276720189));
#33656=CARTESIAN_POINT('Ctrl Pts',(81.9167257663728,-1.85677968476737,339.55635622934));
#33657=CARTESIAN_POINT('Ctrl Pts',(81.9089770758152,-1.72830952401897,339.604576989441));
#33658=CARTESIAN_POINT('Ctrl Pts',(81.9012299974373,-1.59986609256052,339.652787716809));
#33659=CARTESIAN_POINT('Ctrl Pts',(81.8934829190595,-1.46937131797668,339.695632261179));
#33660=CARTESIAN_POINT('Ctrl Pts',(81.8857358406816,-1.33731429046325,339.732945547016));
#33661=CARTESIAN_POINT('Ctrl Pts',(81.8779886973758,-1.20525615618473,339.770259145575));
#33662=CARTESIAN_POINT('Ctrl Pts',(81.87024155407,-1.07163611900863,339.802041286857));
#33663=CARTESIAN_POINT('Ctrl Pts',(81.8624944107642,-0.936957425638541,
339.828177072668));
#33664=CARTESIAN_POINT('Ctrl Pts',(81.854745525736,-0.802248453638783,339.854318734359));
#33665=CARTESIAN_POINT('Ctrl Pts',(81.8469966407079,-0.666480735475762,
339.874811440123));
#33666=CARTESIAN_POINT('Ctrl Pts',(81.8392477556798,-0.53016628429876,339.889591677583));
#33667=CARTESIAN_POINT('Ctrl Pts',(81.8314906459051,-0.393707147555073,
339.90438760294));
#33668=CARTESIAN_POINT('Ctrl Pts',(81.8237335361304,-0.25670050778807,339.913458905834));
#33669=CARTESIAN_POINT('Ctrl Pts',(81.8159764263556,-0.119662614464011,
339.916794069432));
#33670=CARTESIAN_POINT('Ctrl Pts',(81.8082151714295,0.0174485075283376,
339.920131015234));
#33671=CARTESIAN_POINT('Ctrl Pts',(81.8004539165033,0.154590525739848,339.917725720884));
#33672=CARTESIAN_POINT('Ctrl Pts',(81.7926926615771,0.291249633544186,339.909618795127));
#33673=CARTESIAN_POINT('Ctrl Pts',(81.7849189911725,0.428127351384097,339.90149890093));
#33674=CARTESIAN_POINT('Ctrl Pts',(81.7771453207678,0.56452022605252,339.887659188843));
#33675=CARTESIAN_POINT('Ctrl Pts',(81.7693716503631,0.699921107102996,339.868192016173));
#33676=CARTESIAN_POINT('Ctrl Pts',(81.7619598461861,0.829019044564086,339.849631045075));
#33677=CARTESIAN_POINT('Ctrl Pts',(81.7545480420091,0.957214981620196,339.825954791827));
#33678=CARTESIAN_POINT('Ctrl Pts',(81.747136237832,1.08408180987539,339.797285658786));
#33679=CARTESIAN_POINT('Ctrl Pts',(81.7393611590536,1.21716675930101,339.767211366134));
#33680=CARTESIAN_POINT('Ctrl Pts',(81.7315860802752,1.34920959147742,339.731547346251));
#33681=CARTESIAN_POINT('Ctrl Pts',(81.7238110014968,1.47970455936062,339.690379246874));
#33682=CARTESIAN_POINT('Ctrl Pts',(81.7160454904478,1.61003894487804,339.649261807464));
#33683=CARTESIAN_POINT('Ctrl Pts',(81.7082799793987,1.7388288867988,339.602653881602));
#33684=CARTESIAN_POINT('Ctrl Pts',(81.7005144683497,1.86557888138739,339.550692090201));
#33685=CARTESIAN_POINT('Ctrl Pts',(81.6927566568275,1.9922032029874,339.498781819068));
#33686=CARTESIAN_POINT('Ctrl Pts',(81.6849988453054,2.11679124303774,339.441528393669));
#33687=CARTESIAN_POINT('Ctrl Pts',(81.6772410337832,2.23886306514453,339.379118089071));
#33688=CARTESIAN_POINT('Ctrl Pts',(81.6694890602602,2.3608430243339,339.316754750207));
#33689=CARTESIAN_POINT('Ctrl Pts',(81.6617370867372,2.48031018794034,339.249242433732));
#33690=CARTESIAN_POINT('Ctrl Pts',(81.6539851132142,2.59680533906907,339.176815185459));
#33691=CARTESIAN_POINT('Ctrl Pts',(81.6462364226566,2.71325115443222,339.104418610169));
#33692=CARTESIAN_POINT('Ctrl Pts',(81.6384877320989,2.82672712942346,339.027111448941));
#33693=CARTESIAN_POINT('Ctrl Pts',(81.6307390415413,2.93679957093414,338.945173170174));
#33694=CARTESIAN_POINT('Ctrl Pts',(81.6229919631635,3.04684911095401,338.863251939351));
#33695=CARTESIAN_POINT('Ctrl Pts',(81.6152448847857,3.15349621267817,338.776701740797));
#33696=CARTESIAN_POINT('Ctrl Pts',(81.6074978064078,3.25633738580112,338.685844529051));
#33697=CARTESIAN_POINT('Ctrl Pts',(81.599750663102,3.3591794208323,338.594986555833));
#33698=CARTESIAN_POINT('Ctrl Pts',(81.5920035197962,3.45821517071081,338.49982175622));
#33699=CARTESIAN_POINT('Ctrl Pts',(81.5842563764904,3.55307567942612,338.400711143095));
#33700=CARTESIAN_POINT('Ctrl Pts',(81.5765074914623,3.6479575147976,338.3015782478));
#33701=CARTESIAN_POINT('Ctrl Pts',(81.5687586064342,3.73866197091567,338.19849805608));
#33702=CARTESIAN_POINT('Ctrl Pts',(81.5610097214061,3.82485855917157,338.091866760524));
#33703=CARTESIAN_POINT('Ctrl Pts',(81.5532526116314,3.91114663737677,337.985122285409));
#33704=CARTESIAN_POINT('Ctrl Pts',(81.5454955018567,3.99291704372569,337.874819481628));
#33705=CARTESIAN_POINT('Ctrl Pts',(81.5377383920819,4.06988072125754,337.761386241951));
#33706=CARTESIAN_POINT('Ctrl Pts',(81.5299771371558,4.14688552571796,337.647892387177));
#33707=CARTESIAN_POINT('Ctrl Pts',(81.5222158822296,4.21907827764614,337.531265095478));
#33708=CARTESIAN_POINT('Ctrl Pts',(81.5144546273034,4.28621507555429,337.411958413529));
#33709=CARTESIAN_POINT('Ctrl Pts',(81.5066809568987,4.35345927045917,337.29246087977));
#33710=CARTESIAN_POINT('Ctrl Pts',(81.4989072864941,4.41563117201215,337.170275739314));
#33711=CARTESIAN_POINT('Ctrl Pts',(81.4911336160895,4.47253399723777,337.04587944563));
#33712=CARTESIAN_POINT('Ctrl Pts',(81.4837218119123,4.52678798225952,336.927273829344));
#33713=CARTESIAN_POINT('Ctrl Pts',(81.4763100077352,4.57625229321613,336.806658551757));
#33714=CARTESIAN_POINT('Ctrl Pts',(81.4688982035581,4.62079872799927,336.684459016367));
#33715=CARTESIAN_POINT('Ctrl Pts',(81.4611231247796,4.66752851624786,336.556270117735));
#33716=CARTESIAN_POINT('Ctrl Pts',(81.4533480460012,4.70899383417673,336.425932635588));
#33717=CARTESIAN_POINT('Ctrl Pts',(81.4455729672227,4.74499301604917,336.293918212309));
#33718=CARTESIAN_POINT('Ctrl Pts',(81.4378074561737,4.78094789863643,336.162066241182));
#33719=CARTESIAN_POINT('Ctrl Pts',(81.4300419451247,4.81144992698098,336.028541808362));
#33720=CARTESIAN_POINT('Ctrl Pts',(81.4222764340757,4.83634584302084,335.893835526926));
#33721=CARTESIAN_POINT('Ctrl Pts',(81.4145186225535,4.86121707468753,335.75926280716));
#33722=CARTESIAN_POINT('Ctrl Pts',(81.4067608110313,4.88049318515305,335.623510952628));
#33723=CARTESIAN_POINT('Ctrl Pts',(81.3990029995091,4.89407109597274,335.48708435621));
#33724=CARTESIAN_POINT('Ctrl Pts',(81.3912510259861,4.90763878898393,335.350760425132));
#33725=CARTESIAN_POINT('Ctrl Pts',(81.3834990524631,4.91551677900002,335.213763150234));
#33726=CARTESIAN_POINT('Ctrl Pts',(81.3757470789401,4.91765337152596,335.07660535242));
#33727=CARTESIAN_POINT('Ctrl Pts',(81.3679983883825,4.91978905920369,334.939505641014));
#33728=CARTESIAN_POINT('Ctrl Pts',(81.3602496978249,4.91618817936859,334.802245931916));
#33729=CARTESIAN_POINT('Ctrl Pts',(81.3525010072673,4.90685104673398,334.665342163299));
#33730=CARTESIAN_POINT('Ctrl Pts',(81.3447539288894,4.8975158567678,334.528466878654));
#33731=CARTESIAN_POINT('Ctrl Pts',(81.3370068505116,4.8824468144889,334.391947776912));
#33732=CARTESIAN_POINT('Ctrl Pts',(81.3292597721338,4.86169630657989,334.256298389751));
#33733=CARTESIAN_POINT('Ctrl Pts',(81.321512628828,4.84094562476162,334.120647865717));
#33734=CARTESIAN_POINT('Ctrl Pts',(81.3137654855222,4.81451344144438,333.985867457184));
#33735=CARTESIAN_POINT('Ctrl Pts',(81.3060183422164,4.78250367679576,333.852462791917));
#33736=CARTESIAN_POINT('Ctrl Pts',(81.2982694571882,4.75048671567238,333.719028134449));
#33737=CARTESIAN_POINT('Ctrl Pts',(81.2905205721602,4.71288976916171,333.586970215724));
#33738=CARTESIAN_POINT('Ctrl Pts',(81.282771687132,4.66986715771378,333.456781353208));
#33739=CARTESIAN_POINT('Ctrl Pts',(81.2750145773573,4.62679888162173,333.326454306889));
#33740=CARTESIAN_POINT('Ctrl Pts',(81.2672574675826,4.57829355957558,333.198000651395));
#33741=CARTESIAN_POINT('Ctrl Pts',(81.2595003578078,4.52455459042647,333.071895018224));
#33742=CARTESIAN_POINT('Ctrl Pts',(81.2517391028817,4.47078690489034,332.945721998233));
#33743=CARTESIAN_POINT('Ctrl Pts',(81.2439778479555,4.41178016765363,332.821899853361));
#33744=CARTESIAN_POINT('Ctrl Pts',(81.2362165930293,4.34778420716243,332.70087939628));
#33745=CARTESIAN_POINT('Ctrl Pts',(81.2284429226247,4.28368587399077,332.579665345909));
#33746=CARTESIAN_POINT('Ctrl Pts',(81.22066925222,4.21458256602889,332.461262277031));
#33747=CARTESIAN_POINT('Ctrl Pts',(81.2128955818153,4.1407684526044,332.34609350496));
#33748=CARTESIAN_POINT('Ctrl Pts',(81.2054837776383,4.07039040391877,332.236285866937));
#33749=CARTESIAN_POINT('Ctrl Pts',(81.1980719734612,3.99573042070206,332.129418424974));
#33750=CARTESIAN_POINT('Ctrl Pts',(81.1906601692842,3.9170768563161,332.025829197203));
#33751=CARTESIAN_POINT('Ctrl Pts',(81.1828850905057,3.83456824644225,331.917162752801));
#33752=CARTESIAN_POINT('Ctrl Pts',(81.1751100117273,3.74740393988715,331.811760591978));
#33753=CARTESIAN_POINT('Ctrl Pts',(81.1673349329489,3.65587141789133,331.71004753251));
#33754=CARTESIAN_POINT('Ctrl Pts',(81.1595694218999,3.56445153249132,331.608459637437));
#33755=CARTESIAN_POINT('Ctrl Pts',(81.1518039108509,3.46867438605709,331.510552098841));
#33756=CARTESIAN_POINT('Ctrl Pts',(81.1440383998019,3.3688696088616,331.416719293582));
#33757=CARTESIAN_POINT('Ctrl Pts',(81.1362805882797,3.26916378839321,331.322979523823));
#33758=CARTESIAN_POINT('Ctrl Pts',(81.1285227767575,3.16543856721465,331.233306713367));
#33759=CARTESIAN_POINT('Ctrl Pts',(81.1207649652353,3.05806231839768,331.148060499009));
#33760=CARTESIAN_POINT('Ctrl Pts',(81.1130129917123,2.95076687361304,331.06287843513));
#33761=CARTESIAN_POINT('Ctrl Pts',(81.1052610181893,2.83982617487986,330.982116578907));
#33762=CARTESIAN_POINT('Ctrl Pts',(81.0975090446663,2.7256434893779,330.906095918159));
#33763=CARTESIAN_POINT('Ctrl Pts',(81.0897603541086,2.61150916031104,330.830107452207));
#33764=CARTESIAN_POINT('Ctrl Pts',(81.082011663551,2.49413589992537,330.758856404328));
#33765=CARTESIAN_POINT('Ctrl Pts',(81.0742629729934,2.3739577419484,330.692621713624));
#33766=CARTESIAN_POINT('Ctrl Pts',(81.0665158946156,2.25380458804079,330.626400803601));
#33767=CARTESIAN_POINT('Ctrl Pts',(81.0587688162377,2.13084803943928,330.565194363319));
#33768=CARTESIAN_POINT('Ctrl Pts',(81.0510217378599,2.00554828532923,330.50923624116));
#33769=CARTESIAN_POINT('Ctrl Pts',(81.0432745945541,1.88024748108672,330.453277650017));
#33770=CARTESIAN_POINT('Ctrl Pts',(81.0355274512483,1.75260378906572,330.402567624119));
#33771=CARTESIAN_POINT('Ctrl Pts',(81.0277803079425,1.62309863960799,330.357292398976));
#33772=CARTESIAN_POINT('Ctrl Pts',(81.0200314229144,1.49356437464345,330.312006995002));
#33773=CARTESIAN_POINT('Ctrl Pts',(81.0122825378863,1.36216818838727,330.272158952115));
#33774=CARTESIAN_POINT('Ctrl Pts',(81.0045336528582,1.22940759274902,330.237884920186));
#33775=CARTESIAN_POINT('Ctrl Pts',(80.9967765430835,1.09650608364262,330.203574509445));
#33776=CARTESIAN_POINT('Ctrl Pts',(80.9890194333088,0.962237651305697,330.174850025913));
#33777=CARTESIAN_POINT('Ctrl Pts',(80.9812623235341,0.827111494277802,330.151797277492));
#33778=CARTESIAN_POINT('Ctrl Pts',(80.9735010686079,0.691913130151995,330.12873221042));
#33779=CARTESIAN_POINT('Ctrl Pts',(80.9657398136817,0.555856515574606,330.111344967112));
#33780=CARTESIAN_POINT('Ctrl Pts',(80.9579785587555,0.419455945048126,330.099669422104));
#33781=CARTESIAN_POINT('Ctrl Pts',(80.9502048883509,0.282837178061739,330.087975200029));
#33782=CARTESIAN_POINT('Ctrl Pts',(80.9424312179462,0.145873746338524,330.082010951412));
#33783=CARTESIAN_POINT('Ctrl Pts',(80.9346575475415,0.00908081665911037,
330.081758383195));
#33784=CARTESIAN_POINT('Ctrl Pts',(80.9272457433645,-0.121344369233158,
330.08151757209));
#33785=CARTESIAN_POINT('Ctrl Pts',(80.9198339391874,-0.25161428200463,330.086468639879));
#33786=CARTESIAN_POINT('Ctrl Pts',(80.9124221350103,-0.381288630447359,
330.096552025075));
#33787=CARTESIAN_POINT('Ctrl Pts',(80.9046470562319,-0.517318704987591,
330.107129627017));
#33788=CARTESIAN_POINT('Ctrl Pts',(80.8968719774534,-0.653123238444214,
330.123388794772));
#33789=CARTESIAN_POINT('Ctrl Pts',(80.889096898675,-0.788189419890629,330.145317672507));
#33790=CARTESIAN_POINT('Ctrl Pts',(80.881331387626,-0.923089393801948,330.167219565362));
#33791=CARTESIAN_POINT('Ctrl Pts',(80.8735658765769,-1.05725244140097,330.194777224046));
#33792=CARTESIAN_POINT('Ctrl Pts',(80.8658003655279,-1.19016854091595,330.227926875381));
#33793=CARTESIAN_POINT('Ctrl Pts',(80.8580425540057,-1.32295285373191,330.26104365874));
#33794=CARTESIAN_POINT('Ctrl Pts',(80.8502847424834,-1.45449230206158,330.299741306947));
#33795=CARTESIAN_POINT('Ctrl Pts',(80.8425269309612,-1.58428511184755,330.343904667334));
#33796=CARTESIAN_POINT('Ctrl Pts',(80.8347749574382,-1.71398024842757,330.38803479339));
#33797=CARTESIAN_POINT('Ctrl Pts',(80.8270229839152,-1.84193099416484,330.437622319255));
#33798=CARTESIAN_POINT('Ctrl Pts',(80.8192710103921,-1.96764919254343,330.492501833879));
#33799=CARTESIAN_POINT('Ctrl Pts',(80.8115223198345,-2.0933141491902,330.547358106997));
#33800=CARTESIAN_POINT('Ctrl Pts',(80.8037736292769,-2.21674808149705,330.607501755312));
#33801=CARTESIAN_POINT('Ctrl Pts',(80.7960249387193,-2.33748154306765,330.672718740558));
#33802=CARTESIAN_POINT('Ctrl Pts',(80.7882778603414,-2.45818988503319,330.737922156865));
#33803=CARTESIAN_POINT('Ctrl Pts',(80.7805307819636,-2.57619853014122,330.808196624886));
#33804=CARTESIAN_POINT('Ctrl Pts',(80.7727837035857,-2.69106179552668,330.883281710494));
#33805=CARTESIAN_POINT('Ctrl Pts',(80.7650365602799,-2.80592602357709,330.958367425386));
#33806=CARTESIAN_POINT('Ctrl Pts',(80.7572894169741,-2.91764449215216,331.038263624411));
#33807=CARTESIAN_POINT('Ctrl Pts',(80.7495422736683,-3.02580006225466,331.122666245245));
#33808=CARTESIAN_POINT('Ctrl Pts',(80.7417933886402,-3.13397994802509,331.20708784158));
#33809=CARTESIAN_POINT('Ctrl Pts',(80.7340445036122,-3.23859503330414,331.296017635331));
#33810=CARTESIAN_POINT('Ctrl Pts',(80.7262956185841,-3.33926117405886,331.389111207206));
#33811=CARTESIAN_POINT('Ctrl Pts',(80.7185385088094,-3.44003416289565,331.482303589561));
#33812=CARTESIAN_POINT('Ctrl Pts',(80.7107813990346,-3.53684954696647,331.579668312554));
#33813=CARTESIAN_POINT('Ctrl Pts',(80.7030242892599,-3.62935961202736,331.680823615852));
#33814=CARTESIAN_POINT('Ctrl Pts',(80.6952630343338,-3.72191911150887,331.78203297331));
#33815=CARTESIAN_POINT('Ctrl Pts',(80.6875017794076,-3.81016845642133,331.887036648114));
#33816=CARTESIAN_POINT('Ctrl Pts',(80.6797405244815,-3.89380084667984,331.995420490502));
#33817=CARTESIAN_POINT('Ctrl Pts',(80.6719668540768,-3.97756702150725,332.103977711716));
#33818=CARTESIAN_POINT('Ctrl Pts',(80.6641931836722,-4.05670125727636,332.215925586283));
#33819=CARTESIAN_POINT('Ctrl Pts',(80.6564195132675,-4.13094015070425,332.330821000045));
#33820=CARTESIAN_POINT('Ctrl Pts',(80.6490077090904,-4.20172320578218,332.440368004654));
#33821=CARTESIAN_POINT('Ctrl Pts',(80.6415959049133,-4.26805627193853,332.552594060364));
#33822=CARTESIAN_POINT('Ctrl Pts',(80.6341841007362,-4.3297511688621,332.667096684764));
#33823=CARTESIAN_POINT('Ctrl Pts',(80.6259892272813,-4.39796423291835,332.79369669939));
#33824=CARTESIAN_POINT('Ctrl Pts',(80.6177943538264,-4.46070386279604,332.923444483748));
#33825=CARTESIAN_POINT('Ctrl Pts',(80.6095994803714,-4.51768456457364,333.055852567959));
#33826=CARTESIAN_POINT('Ctrl Pts',(80.60141900125,-4.57456517948293,333.188028076752));
#33827=CARTESIAN_POINT('Ctrl Pts',(80.5932385221284,-4.62570689507404,333.322854273003));
#33828=CARTESIAN_POINT('Ctrl Pts',(80.5850580430069,-4.67086986338482,333.459818912652));
#33829=CARTESIAN_POINT('Ctrl Pts',(80.5768967514728,-4.71592690044302,333.596462297159));
#33830=CARTESIAN_POINT('Ctrl Pts',(80.5687354599387,-4.75503305256771,333.735233811639));
#33831=CARTESIAN_POINT('Ctrl Pts',(80.5605741684045,-4.78799664016023,333.875601833729));
#33832=CARTESIAN_POINT('Ctrl Pts',(80.5524243534081,-4.82091387383258,334.015772468077));
#33833=CARTESIAN_POINT('Ctrl Pts',(80.5442745384117,-4.84770567721586,334.157534818817));
#33834=CARTESIAN_POINT('Ctrl Pts',(80.5361247234153,-4.86822969881815,334.300341038759));
#33835=CARTESIAN_POINT('Ctrl Pts',(80.5279900893834,-4.88871548955942,334.442881248225));
#33836=CARTESIAN_POINT('Ctrl Pts',(80.5198554553515,-4.90295673280841,334.586461125167));
#33837=CARTESIAN_POINT('Ctrl Pts',(80.5117208213197,-4.91086191365771,334.7305221206));
#33838=CARTESIAN_POINT('Ctrl Pts',(80.5066592970536,-4.91578066778231,334.820159616437));
#33839=CARTESIAN_POINT('Ctrl Pts',(80.5015977727876,-4.91824737078159,334.909983125481));
#33840=CARTESIAN_POINT('Ctrl Pts',(80.4965362485215,-4.91824999789874,334.999856232645));
#33841=CARTESIAN_POINT('',(83.9965362485267,-4.91824940115574,335.002427041657));
#33842=CARTESIAN_POINT('Ctrl Pts',(83.99653624849,-4.91824940115542,335.002427042302));
#33843=CARTESIAN_POINT('Ctrl Pts',(83.9887043363345,-4.91818150444409,335.140015480526));
#33844=CARTESIAN_POINT('Ctrl Pts',(83.980872424179,-4.91234057685994,335.277456908605));
#33845=CARTESIAN_POINT('Ctrl Pts',(83.9730405120234,-4.90076020166624,335.414406211662));
#33846=CARTESIAN_POINT('Ctrl Pts',(83.965265433245,-4.88926386110129,335.550361722752));
#33847=CARTESIAN_POINT('Ctrl Pts',(83.9574903544666,-4.87208760806765,335.686053314884));
#33848=CARTESIAN_POINT('Ctrl Pts',(83.9497152756881,-4.84924676253089,335.820968268926));
#33849=CARTESIAN_POINT('Ctrl Pts',(83.9419497646391,-4.82643402410869,335.955717201529));
#33850=CARTESIAN_POINT('Ctrl Pts',(83.9341842535901,-4.79797062738378,336.089691015911));
#33851=CARTESIAN_POINT('Ctrl Pts',(83.9264187425411,-4.76392378964062,336.222380132772));
#33852=CARTESIAN_POINT('Ctrl Pts',(83.9186609310189,-4.72991070943618,336.354937687988));
#33853=CARTESIAN_POINT('Ctrl Pts',(83.9109031194967,-4.69032530168452,336.48621270441));
#33854=CARTESIAN_POINT('Ctrl Pts',(83.9031453079745,-4.64528610626961,336.61570419737));
#33855=CARTESIAN_POINT('Ctrl Pts',(83.8953933344515,-4.60028080427757,336.745098243874));
#33856=CARTESIAN_POINT('Ctrl Pts',(83.8876413609285,-4.54983001161845,336.872711070722));
#33857=CARTESIAN_POINT('Ctrl Pts',(83.8798893874055,-4.49410243340968,336.998055650006));
#33858=CARTESIAN_POINT('Ctrl Pts',(83.8721406968479,-4.43839845586336,337.123347145786));
#33859=CARTESIAN_POINT('Ctrl Pts',(83.8643920062903,-4.37742229593515,337.246371948155));
#33860=CARTESIAN_POINT('Ctrl Pts',(83.8566433157327,-4.31139115845305,337.366662067409));
#33861=CARTESIAN_POINT('Ctrl Pts',(83.8488962373549,-4.24537375930056,337.486927159299));
#33862=CARTESIAN_POINT('Ctrl Pts',(83.841149158977,-4.17430366253076,337.604458357375));
#33863=CARTESIAN_POINT('Ctrl Pts',(83.8334020805992,-4.09844430723293,337.718811748358));
#33864=CARTESIAN_POINT('Ctrl Pts',(83.8256549372934,-4.02258431616073,337.833166097733));
#33865=CARTESIAN_POINT('Ctrl Pts',(83.8179077939876,-3.94193520257662,337.944342261174));
#33866=CARTESIAN_POINT('Ctrl Pts',(83.8101606506818,-3.85680383993657,338.05192516336));
#33867=CARTESIAN_POINT('Ctrl Pts',(83.8024117656537,-3.7716533379588,338.159532252467));
#33868=CARTESIAN_POINT('Ctrl Pts',(83.7946628806256,-3.68201882420734,338.263544166348));
#33869=CARTESIAN_POINT('Ctrl Pts',(83.7869139955975,-3.58824730528171,338.363579096534));
#33870=CARTESIAN_POINT('Ctrl Pts',(83.7791568858228,-3.49437625629705,338.463720204828));
#33871=CARTESIAN_POINT('Ctrl Pts',(83.7713997760481,-3.39635969832406,338.559875611538));
#33872=CARTESIAN_POINT('Ctrl Pts',(83.7636426662733,-3.29458173204331,338.651700189417));
#33873=CARTESIAN_POINT('Ctrl Pts',(83.7558814113472,-3.19274937887168,338.743573835414));
#33874=CARTESIAN_POINT('Ctrl Pts',(83.748120156421,-3.08715191310231,338.831111791885));
#33875=CARTESIAN_POINT('Ctrl Pts',(83.7403589014949,-2.97820554770165,338.914010063623));
#33876=CARTESIAN_POINT('Ctrl Pts',(83.7325852310902,-2.86908490362181,338.997040945579));
#33877=CARTESIAN_POINT('Ctrl Pts',(83.7248115606856,-2.75660497560906,339.0754170879));
#33878=CARTESIAN_POINT('Ctrl Pts',(83.7170378902809,-2.64121064718774,339.148878086867));
#33879=CARTESIAN_POINT('Ctrl Pts',(83.7096260861038,-2.53118795251655,339.218919458658));
#33880=CARTESIAN_POINT('Ctrl Pts',(83.7022142819267,-2.41851633072506,339.284492844179));
#33881=CARTESIAN_POINT('Ctrl Pts',(83.6948024777496,-2.30359952632896,339.345412786468));
#33882=CARTESIAN_POINT('Ctrl Pts',(83.6870273989712,-2.18305030703007,339.4093185966));
#33883=CARTESIAN_POINT('Ctrl Pts',(83.6792523201928,-2.05964929626415,339.468305225468));
#33884=CARTESIAN_POINT('Ctrl Pts',(83.6714772414143,-1.9338359409981,339.522108094219));
#33885=CARTESIAN_POINT('Ctrl Pts',(83.6637117303653,-1.80817740707538,339.575844755115));
#33886=CARTESIAN_POINT('Ctrl Pts',(83.6559462193163,-1.68011279115845,339.624410195947));
#33887=CARTESIAN_POINT('Ctrl Pts',(83.6481807082673,-1.55010698448145,339.667585178565));
#33888=CARTESIAN_POINT('Ctrl Pts',(83.6404228967451,-1.42023007894028,339.710717353062));
#33889=CARTESIAN_POINT('Ctrl Pts',(83.6326650852229,-1.28841618145678,339.748469583111));
#33890=CARTESIAN_POINT('Ctrl Pts',(83.6249072737007,-1.15515072945985,339.780670439879));
#33891=CARTESIAN_POINT('Ctrl Pts',(83.6171553001777,-1.02198556394173,339.81284706448));
#33892=CARTESIAN_POINT('Ctrl Pts',(83.6094033266547,-0.887371396571579,
339.839480539642));
#33893=CARTESIAN_POINT('Ctrl Pts',(83.6016513531317,-0.751809075525826,
339.860449174352));
#33894=CARTESIAN_POINT('Ctrl Pts',(83.5939026625741,-0.616304165203521,
339.881408928832));
#33895=CARTESIAN_POINT('Ctrl Pts',(83.5861539720164,-0.479852285324325,
339.896708554803));
#33896=CARTESIAN_POINT('Ctrl Pts',(83.5784052814588,-0.342964520408958,
339.906277448355));
#33897=CARTESIAN_POINT('Ctrl Pts',(83.570658203081,-0.206105236136298,339.91584435102));
#33898=CARTESIAN_POINT('Ctrl Pts',(83.5629111247032,-0.0688106368933147,
339.91968286565));
#33899=CARTESIAN_POINT('Ctrl Pts',(83.5551640463253,0.0684034191679079,
339.917774296849));
#33900=CARTESIAN_POINT('Ctrl Pts',(83.5474169030195,0.205618625214894,339.915865712052));
#33901=CARTESIAN_POINT('Ctrl Pts',(83.5396697597137,0.342752895897242,339.908209953191));
#33902=CARTESIAN_POINT('Ctrl Pts',(83.5319226164079,0.479291118687179,339.894840455628));
#33903=CARTESIAN_POINT('Ctrl Pts',(83.5241737313798,0.615860038168481,339.881467952317));
#33904=CARTESIAN_POINT('Ctrl Pts',(83.5164248463517,0.751832254166132,339.862379192239));
#33905=CARTESIAN_POINT('Ctrl Pts',(83.5086759613236,0.886698910610572,339.837659362173));
#33906=CARTESIAN_POINT('Ctrl Pts',(83.5009188515489,1.0217087159176,339.812913294225));
#33907=CARTESIAN_POINT('Ctrl Pts',(83.4931617417742,1.15561023251362,339.782524287501));
#33908=CARTESIAN_POINT('Ctrl Pts',(83.4854046319995,1.28790537661639,339.746628572301));
#33909=CARTESIAN_POINT('Ctrl Pts',(83.4776433770733,1.42027121501409,339.710713675579));
#33910=CARTESIAN_POINT('Ctrl Pts',(83.4698821221471,1.55102859806014,339.669286324963));
#33911=CARTESIAN_POINT('Ctrl Pts',(83.462120867221,1.67969665298089,339.622532013568));
#33912=CARTESIAN_POINT('Ctrl Pts',(83.4543471968163,1.80857053485679,339.575702910512));
#33913=CARTESIAN_POINT('Ctrl Pts',(83.4465735264117,1.93534804816124,339.523529967225));
#33914=CARTESIAN_POINT('Ctrl Pts',(83.438799856007,2.05956946184786,339.466246376357));
#33915=CARTESIAN_POINT('Ctrl Pts',(83.4313880518299,2.17800833884226,339.411629350426));
#33916=CARTESIAN_POINT('Ctrl Pts',(83.4239762476527,2.29412347732198,339.352366901423));
#33917=CARTESIAN_POINT('Ctrl Pts',(83.4165644434756,2.40754043324713,339.288698185322));
#33918=CARTESIAN_POINT('Ctrl Pts',(83.4087893646972,2.52651629203309,339.221908875785));
#33919=CARTESIAN_POINT('Ctrl Pts',(83.4010142859187,2.64289877434749,339.15005938272));
#33920=CARTESIAN_POINT('Ctrl Pts',(83.3932392071403,2.7562275802174,339.073376067656));
#33921=CARTESIAN_POINT('Ctrl Pts',(83.3854736960913,2.86941692777683,338.996787116292));
#33922=CARTESIAN_POINT('Ctrl Pts',(83.3777081850423,2.97955975508958,338.915376395347));
#33923=CARTESIAN_POINT('Ctrl Pts',(83.3699426739933,3.08622012079563,338.829416199435));
#33924=CARTESIAN_POINT('Ctrl Pts',(83.3621848624711,3.19277473243855,338.743541233307));
#33925=CARTESIAN_POINT('Ctrl Pts',(83.3544270509489,3.29585345150338,338.653126012689));
#33926=CARTESIAN_POINT('Ctrl Pts',(83.3466692394267,3.39504942177975,338.558485982293));
#33927=CARTESIAN_POINT('Ctrl Pts',(83.3389172659037,3.49417074394273,338.46391717152));
#33928=CARTESIAN_POINT('Ctrl Pts',(83.3311652923807,3.5894148515303,338.36513014795));
#33929=CARTESIAN_POINT('Ctrl Pts',(83.3234133188577,3.68040837428604,338.262480231509));
#33930=CARTESIAN_POINT('Ctrl Pts',(83.3156646283001,3.77136336123088,338.159873787368));
#33931=CARTESIAN_POINT('Ctrl Pts',(83.3079159377425,3.85807108492248,338.053407996009));
#33932=CARTESIAN_POINT('Ctrl Pts',(83.3001672471848,3.94019559586849,337.943474431484));
#33933=CARTESIAN_POINT('Ctrl Pts',(83.292420168807,4.02230302012408,337.833563739555));
#33934=CARTESIAN_POINT('Ctrl Pts',(83.2846730904292,4.09982889457998,337.720187022519));
#33935=CARTESIAN_POINT('Ctrl Pts',(83.2769260120513,4.17247833743341,337.603767959352));
#33936=CARTESIAN_POINT('Ctrl Pts',(83.2691788687455,4.24512838915914,337.487347920481));
#33937=CARTESIAN_POINT('Ctrl Pts',(83.2614317254397,4.31290172083319,337.367885816226));
#33938=CARTESIAN_POINT('Ctrl Pts',(83.2536845821339,4.37554769201968,337.245832909493));
#33939=CARTESIAN_POINT('Ctrl Pts',(83.2459356971058,4.43820774735042,337.123752562676));
#33940=CARTESIAN_POINT('Ctrl Pts',(83.2381868120778,4.49573796991978,336.999080602012));
#33941=CARTESIAN_POINT('Ctrl Pts',(83.2304379270497,4.54793462389251,336.872291034882));
#33942=CARTESIAN_POINT('Ctrl Pts',(83.222680817275,4.60018667993312,336.745366891995));
#33943=CARTESIAN_POINT('Ctrl Pts',(83.2149237075002,4.64709370975516,336.616321014767));
#33944=CARTESIAN_POINT('Ctrl Pts',(83.2071665977255,4.68850073060997,336.485645974507));
#33945=CARTESIAN_POINT('Ctrl Pts',(83.1994053427993,4.72992987805278,336.354901105684));
#33946=CARTESIAN_POINT('Ctrl Pts',(83.1916440878731,4.76585305792996,336.222525716176));
#33947=CARTESIAN_POINT('Ctrl Pts',(83.183882832947,4.79616602750741,336.089024563122));
#33948=CARTESIAN_POINT('Ctrl Pts',(83.1761091625423,4.82652748795718,335.955309851732));
#33949=CARTESIAN_POINT('Ctrl Pts',(83.1683354921377,4.85126073382683,335.820466162819));
#33950=CARTESIAN_POINT('Ctrl Pts',(83.160561821733,4.87031307494354,335.685006287952));
#33951=CARTESIAN_POINT('Ctrl Pts',(83.1531500175559,4.88847852499755,335.55585210285));
#33952=CARTESIAN_POINT('Ctrl Pts',(83.1457382133789,4.90148003143856,335.426138094061));
#33953=CARTESIAN_POINT('Ctrl Pts',(83.1383264092018,4.90931607247105,335.296308560587));
#33954=CARTESIAN_POINT('Ctrl Pts',(83.1305513304233,4.91753618121691,335.160115694936));
#33955=CARTESIAN_POINT('Ctrl Pts',(83.1227762516449,4.92009764886239,335.023365299226));
#33956=CARTESIAN_POINT('Ctrl Pts',(83.1150011728665,4.91694173291969,334.886566946736));
#33957=CARTESIAN_POINT('Ctrl Pts',(83.1072356618175,4.91378970053247,334.749936933329));
#33958=CARTESIAN_POINT('Ctrl Pts',(83.0994701507685,4.90493429232151,334.613259467598));
#33959=CARTESIAN_POINT('Ctrl Pts',(83.0917046397194,4.89036857375248,334.477048496174));
#33960=CARTESIAN_POINT('Ctrl Pts',(83.0839468281972,4.87581729713584,334.340972578324));
#33961=CARTESIAN_POINT('Ctrl Pts',(83.076189016675,4.85556701873552,334.205362620474));
#33962=CARTESIAN_POINT('Ctrl Pts',(83.0684312051528,4.82966282949875,334.070731461924));
#33963=CARTESIAN_POINT('Ctrl Pts',(83.0606792316298,4.80377813398585,333.93620161759));
#33964=CARTESIAN_POINT('Ctrl Pts',(83.0529272581068,4.77224807005836,333.802649488724));
#33965=CARTESIAN_POINT('Ctrl Pts',(83.0451752845838,4.73516938175326,333.67058133434));
#33966=CARTESIAN_POINT('Ctrl Pts',(83.0374265940262,4.69810639629466,333.538569110897));
#33967=CARTESIAN_POINT('Ctrl Pts',(83.0296779034685,4.6554995655707,333.408039987506));
#33968=CARTESIAN_POINT('Ctrl Pts',(83.0219292129109,4.6074963710079,333.279488374451));
#33969=CARTESIAN_POINT('Ctrl Pts',(83.0141821345331,4.55950316391067,333.150963507632));
#33970=CARTESIAN_POINT('Ctrl Pts',(83.0064350561553,4.50611596287135,333.024415698718));
#33971=CARTESIAN_POINT('Ctrl Pts',(82.9986879777774,4.44753147111442,332.900322197111));
#33972=CARTESIAN_POINT('Ctrl Pts',(82.9909408344716,4.38894648836302,332.77622765548));
#33973=CARTESIAN_POINT('Ctrl Pts',(82.9831936911658,4.32516429488406,332.654587815648));
#33974=CARTESIAN_POINT('Ctrl Pts',(82.97544654786,4.25642873136212,332.535857650757));
#33975=CARTESIAN_POINT('Ctrl Pts',(82.9676976628319,4.18767771462625,332.417100792804));
#33976=CARTESIAN_POINT('Ctrl Pts',(82.9599487778038,4.11397130766016,332.301255249701));
#33977=CARTESIAN_POINT('Ctrl Pts',(82.9521998927757,4.03559786023181,332.18874885985));
#33978=CARTESIAN_POINT('Ctrl Pts',(82.944442783001,3.95714122641655,332.076123054555));
#33979=CARTESIAN_POINT('Ctrl Pts',(82.9366856732262,3.87400788054348,331.966843803641));
#33980=CARTESIAN_POINT('Ctrl Pts',(82.9289285634515,3.78652816627843,331.861307994008));
#33981=CARTESIAN_POINT('Ctrl Pts',(82.9211673085253,3.6990017056512,331.755715789412));
#33982=CARTESIAN_POINT('Ctrl Pts',(82.9134060535992,3.60712451041142,331.653871302104));
#33983=CARTESIAN_POINT('Ctrl Pts',(82.905644798673,3.51126462988296,331.556135345076));
#33984=CARTESIAN_POINT('Ctrl Pts',(82.8978711282683,3.41525140478632,331.458243042369));
#33985=CARTESIAN_POINT('Ctrl Pts',(82.8900974578636,3.31524304854875,331.364472670856));
#33986=CARTESIAN_POINT('Ctrl Pts',(82.882323787459,3.2116422648649,331.275146039771));
#33987=CARTESIAN_POINT('Ctrl Pts',(82.8749119832819,3.1128641225863,331.189977584853));
#33988=CARTESIAN_POINT('Ctrl Pts',(82.8675001791048,3.0108207064303,331.108848647568));
#33989=CARTESIAN_POINT('Ctrl Pts',(82.8600883749277,2.90588481337507,331.03200094331));
#33990=CARTESIAN_POINT('Ctrl Pts',(82.8523132961493,2.79580569961331,330.951386704148));
#33991=CARTESIAN_POINT('Ctrl Pts',(82.8445382173708,2.68219553153876,330.875229225503));
#33992=CARTESIAN_POINT('Ctrl Pts',(82.8367631385924,2.56545103126276,330.803853664528));
#33993=CARTESIAN_POINT('Ctrl Pts',(82.8289976275434,2.44885019252674,330.732565935725));
#33994=CARTESIAN_POINT('Ctrl Pts',(82.8212321164944,2.32912302620167,330.666048618153));
#33995=CARTESIAN_POINT('Ctrl Pts',(82.8134666054454,2.20669796829874,330.604585669222));
#33996=CARTESIAN_POINT('Ctrl Pts',(82.8057087939232,2.08439429519707,330.543183660984));
#33997=CARTESIAN_POINT('Ctrl Pts',(82.797950982401,1.95939840092588,330.486826222621));
#33998=CARTESIAN_POINT('Ctrl Pts',(82.7901931708788,1.83216594429326,330.435752962966));
#33999=CARTESIAN_POINT('Ctrl Pts',(82.7824411973558,1.70502923411912,330.384718137559));
#34000=CARTESIAN_POINT('Ctrl Pts',(82.7746892238328,1.57565967295978,330.338959720831));
#34001=CARTESIAN_POINT('Ctrl Pts',(82.7669372503098,1.4445353385708,330.298670324459));
#34002=CARTESIAN_POINT('Ctrl Pts',(82.7591885597521,1.31346653541529,330.258397990671));
#34003=CARTESIAN_POINT('Ctrl Pts',(82.7514398691945,1.18064480995528,330.223590185177));
#34004=CARTESIAN_POINT('Ctrl Pts',(82.7436911786369,1.0465657330079,330.194390441474));
#34005=CARTESIAN_POINT('Ctrl Pts',(82.7359441002591,0.912514552332327,330.165196773022));
#34006=CARTESIAN_POINT('Ctrl Pts',(82.7281970218812,0.777206922197701,330.141608928626));
#34007=CARTESIAN_POINT('Ctrl Pts',(82.7204499435034,0.641150619209999,330.123719763387));
#34008=CARTESIAN_POINT('Ctrl Pts',(82.7127028001976,0.505093175939431,330.105830448218));
#34009=CARTESIAN_POINT('Ctrl Pts',(82.7049556568918,0.368287434839402,330.093639958423));
#34010=CARTESIAN_POINT('Ctrl Pts',(82.697208513586,0.231247948717784,330.087189455239));
#34011=CARTESIAN_POINT('Ctrl Pts',(82.6894596285579,0.0941776532105353,
330.080737501846));
#34012=CARTESIAN_POINT('Ctrl Pts',(82.6817107435298,-0.0431261015229156,
330.080028121332));
#34013=CARTESIAN_POINT('Ctrl Pts',(82.6739618585017,-0.180147494437449,
330.085050362135));
#34014=CARTESIAN_POINT('Ctrl Pts',(82.666204748727,-0.317314323274304,330.090077933597));
#34015=CARTESIAN_POINT('Ctrl Pts',(82.6584476389523,-0.45419780038092,330.100849264602));
#34016=CARTESIAN_POINT('Ctrl Pts',(82.6506905291776,-0.590285407183225,
330.117301340389));
#34017=CARTESIAN_POINT('Ctrl Pts',(82.6429292742514,-0.726445734851458,
330.13376220764));
#34018=CARTESIAN_POINT('Ctrl Pts',(82.6351680193252,-0.861808959241969,
330.155909805313));
#34019=CARTESIAN_POINT('Ctrl Pts',(82.627406764399,-0.995872492405019,330.183629889494));
#34020=CARTESIAN_POINT('Ctrl Pts',(82.6196330939944,-1.13015048352984,330.211394316777));
#34021=CARTESIAN_POINT('Ctrl Pts',(82.6118594235897,-1.2631242494764,330.244748948553));
#34022=CARTESIAN_POINT('Ctrl Pts',(82.6040857531851,-1.39430524791927,330.283529292138));
#34023=CARTESIAN_POINT('Ctrl Pts',(82.596673949008,-1.51937973932368,330.320504401398));
#34024=CARTESIAN_POINT('Ctrl Pts',(82.589262144831,-1.64282434122797,330.362411363902));
#34025=CARTESIAN_POINT('Ctrl Pts',(82.5818503406539,-1.7642340481647,330.409067492786));
#34026=CARTESIAN_POINT('Ctrl Pts',(82.5740752618755,-1.89159440649998,330.458010377528));
#34027=CARTESIAN_POINT('Ctrl Pts',(82.566300183097,-2.01711783593588,330.512334410019));
#34028=CARTESIAN_POINT('Ctrl Pts',(82.5585251043186,-2.1403162157879,330.571881939363));
#34029=CARTESIAN_POINT('Ctrl Pts',(82.5507595932696,-2.26336299219023,330.631356191682));
#34030=CARTESIAN_POINT('Ctrl Pts',(82.5429940822206,-2.38409006326298,330.696040982811));
#34031=CARTESIAN_POINT('Ctrl Pts',(82.5352285711716,-2.5020267918532,330.765729697416));
#34032=CARTESIAN_POINT('Ctrl Pts',(82.5274707596494,-2.61984658583374,330.835349315457));
#34033=CARTESIAN_POINT('Ctrl Pts',(82.5197129481272,-2.73488120873949,330.909962785933));
#34034=CARTESIAN_POINT('Ctrl Pts',(82.511955136605,-2.84668258526416,330.989316601718));
#34035=CARTESIAN_POINT('Ctrl Pts',(82.504203163082,-2.95839982770748,331.068610701241));
#34036=CARTESIAN_POINT('Ctrl Pts',(82.496451189559,-3.06688834931433,331.152637820289));
#34037=CARTESIAN_POINT('Ctrl Pts',(82.4886992160359,-3.17172746351039,331.24110016631));
#34038=CARTESIAN_POINT('Ctrl Pts',(82.4809505254783,-3.27652217827935,331.329525048475));
#34039=CARTESIAN_POINT('Ctrl Pts',(82.4732018349207,-3.37767026146619,331.422381170217));
#34040=CARTESIAN_POINT('Ctrl Pts',(82.4654531443631,-3.47478283088745,331.519329469675));
#34041=CARTESIAN_POINT('Ctrl Pts',(82.4577060659852,-3.57187519522748,331.61625759823));
#34042=CARTESIAN_POINT('Ctrl Pts',(82.4499589876074,-3.66493343942012,331.717275934999));
#34043=CARTESIAN_POINT('Ctrl Pts',(82.4422119092296,-3.75360469257444,331.822007729024));
#34044=CARTESIAN_POINT('Ctrl Pts',(82.4344647659238,-3.84227668887914,331.926740400802));
#34045=CARTESIAN_POINT('Ctrl Pts',(82.426717622618,-3.92656136824199,332.035186293597));
#34046=CARTESIAN_POINT('Ctrl Pts',(82.4189704793122,-4.0061456632488,332.146934983683));
#34047=CARTESIAN_POINT('Ctrl Pts',(82.4112215942841,-4.0857478504948,332.258708797247));
#34048=CARTESIAN_POINT('Ctrl Pts',(82.403472709256,-4.16064732387697,332.373786567349));
#34049=CARTESIAN_POINT('Ctrl Pts',(82.3957238242279,-4.23057415243261,332.491728602549));
#34050=CARTESIAN_POINT('Ctrl Pts',(82.3879667144532,-4.30057520204665,332.609795822644));
#34051=CARTESIAN_POINT('Ctrl Pts',(82.3802096046785,-4.36559286384296,332.73073304409));
#34052=CARTESIAN_POINT('Ctrl Pts',(82.3724524949037,-4.42540277506992,332.85407517818));
#34053=CARTESIAN_POINT('Ctrl Pts',(82.3646912399776,-4.485244646801,332.977483222363));
#34054=CARTESIAN_POINT('Ctrl Pts',(82.3569299850514,-4.53987306727684,333.10329838153));
#34055=CARTESIAN_POINT('Ctrl Pts',(82.3491687301252,-4.58911212746512,333.231036194816));
#34056=CARTESIAN_POINT('Ctrl Pts',(82.3413950597206,-4.63842995410276,333.358978346973));
#34057=CARTESIAN_POINT('Ctrl Pts',(82.3336213893159,-4.68234106743871,333.488848928771));
#34058=CARTESIAN_POINT('Ctrl Pts',(82.3258477189113,-4.72071941459793,333.620148098114));
#34059=CARTESIAN_POINT('Ctrl Pts',(82.3184359147341,-4.75731124046394,333.745335259537));
#34060=CARTESIAN_POINT('Ctrl Pts',(82.3110241105569,-4.78887373898933,333.871820720887));
#34061=CARTESIAN_POINT('Ctrl Pts',(82.3036123063798,-4.81534136375698,333.999165042082));
#34062=CARTESIAN_POINT('Ctrl Pts',(82.2926006445855,-4.85466411507003,334.188359543569));
#34063=CARTESIAN_POINT('Ctrl Pts',(82.2815889827912,-4.88284747263759,334.3799424553));
#34064=CARTESIAN_POINT('Ctrl Pts',(82.2705773209969,-4.89966400728638,334.572828280194));
#34065=CARTESIAN_POINT('Ctrl Pts',(82.2625636301613,-4.91190217007419,334.713200132885));
#34066=CARTESIAN_POINT('Ctrl Pts',(82.2545499393256,-4.91812116425913,334.854261771732));
#34067=CARTESIAN_POINT('Ctrl Pts',(82.2465362484899,-4.91824801864458,334.995585297446));
#34068=CARTESIAN_POINT('',(85.746536248436,-4.91824901287694,335.003116060811));
#34069=CARTESIAN_POINT('Ctrl Pts',(85.7465362484359,-4.91824901287694,335.003116060811));
#34070=CARTESIAN_POINT('Ctrl Pts',(85.7378083397602,-4.91815097020962,335.157862158879));
#34071=CARTESIAN_POINT('Ctrl Pts',(85.7290804310845,-4.91074557489866,335.312332150909));
#34072=CARTESIAN_POINT('Ctrl Pts',(85.7203525224088,-4.89613509597295,335.46588001082));
#34073=CARTESIAN_POINT('Ctrl Pts',(85.7115908771786,-4.88146814221046,335.620021389286));
#34074=CARTESIAN_POINT('Ctrl Pts',(85.7028292319484,-4.8595404069818,335.773233305754));
#34075=CARTESIAN_POINT('Ctrl Pts',(85.6940675867182,-4.83050522521385,335.924879630915));
#34076=CARTESIAN_POINT('Ctrl Pts',(85.6852578442456,-4.80131065418298,336.077358421883));
#34077=CARTESIAN_POINT('Ctrl Pts',(85.676448101773,-4.76493048672398,336.228254199914));
#34078=CARTESIAN_POINT('Ctrl Pts',(85.6676383593005,-4.72156937661856,336.376940697444));
#34079=CARTESIAN_POINT('Ctrl Pts',(85.659248478756,-4.68027480584169,336.518540971997));
#34080=CARTESIAN_POINT('Ctrl Pts',(85.6508585982116,-4.63264928898657,336.658137558858));
#34081=CARTESIAN_POINT('Ctrl Pts',(85.6424687176671,-4.57890908465216,336.795208805958));
#34082=CARTESIAN_POINT('Ctrl Pts',(85.6346936388887,-4.52910690689109,336.922235613887));
#34083=CARTESIAN_POINT('Ctrl Pts',(85.6269185601102,-4.47393611394265,337.04738918135));
#34084=CARTESIAN_POINT('Ctrl Pts',(85.6191434813318,-4.41355765070659,337.170182463847));
#34085=CARTESIAN_POINT('Ctrl Pts',(85.6113779702828,-4.35325348701347,337.292824641393));
#34086=CARTESIAN_POINT('Ctrl Pts',(85.6036124592338,-4.28775457467606,337.413111965645));
#34087=CARTESIAN_POINT('Ctrl Pts',(85.5958469481848,-4.21727070380278,337.530575206025));
#34088=CARTESIAN_POINT('Ctrl Pts',(85.5880891366626,-4.14685671789268,337.64792198126));
#34089=CARTESIAN_POINT('Ctrl Pts',(85.5803313251404,-4.07146780932203,337.762449911949));
#34090=CARTESIAN_POINT('Ctrl Pts',(85.5725735136182,-3.99136050649795,337.873712645633));
#34091=CARTESIAN_POINT('Ctrl Pts',(85.5648215400952,-3.9113134869597,337.984891650581));
#34092=CARTESIAN_POINT('Ctrl Pts',(85.5570695665722,-3.82655536821161,338.092810033455));
#34093=CARTESIAN_POINT('Ctrl Pts',(85.5493175930492,-3.73738677804871,338.197049129082));
#34094=CARTESIAN_POINT('Ctrl Pts',(85.5415689024916,-3.64825595083656,338.301244079391));
#34095=CARTESIAN_POINT('Ctrl Pts',(85.533820211934,-3.55471862076062,338.401762545156));
#34096=CARTESIAN_POINT('Ctrl Pts',(85.5260715213764,-3.45711646912184,338.498217943672));
#34097=CARTESIAN_POINT('Ctrl Pts',(85.5183244429985,-3.35953462442589,338.594653273836));
#34098=CARTESIAN_POINT('Ctrl Pts',(85.5105773646207,-3.25788991820788,338.687026943644));
#34099=CARTESIAN_POINT('Ctrl Pts',(85.5028302862429,-3.15256147672356,338.774988635477));
#34100=CARTESIAN_POINT('Ctrl Pts',(85.4950831429371,-3.04723215248559,338.862951064513));
#34101=CARTESIAN_POINT('Ctrl Pts',(85.4873359996313,-2.93821933141674,338.946501191275));
#34102=CARTESIAN_POINT('Ctrl Pts',(85.4795888563255,-2.82593554286927,339.025328728197));
#34103=CARTESIAN_POINT('Ctrl Pts',(85.4718399712974,-2.71362651054221,339.104173987223));
#34104=CARTESIAN_POINT('Ctrl Pts',(85.4640910862693,-2.59804536725416,339.178294319122));
#34105=CARTESIAN_POINT('Ctrl Pts',(85.4563422012412,-2.47963361798748,339.247422769521));
#34106=CARTESIAN_POINT('Ctrl Pts',(85.4485850914665,-2.36109618526671,339.316624593572));
#34107=CARTESIAN_POINT('Ctrl Pts',(85.4408279816918,-2.23972248302163,339.380823754623));
#34108=CARTESIAN_POINT('Ctrl Pts',(85.4330708719171,-2.11597910507516,339.439799037049));
#34109=CARTESIAN_POINT('Ctrl Pts',(85.4253096169909,-1.99216960262406,339.498805833981));
#34110=CARTESIAN_POINT('Ctrl Pts',(85.4175483620647,-1.86598826069384,339.552583036853));
#34111=CARTESIAN_POINT('Ctrl Pts',(85.4097871071386,-1.73792071748697,339.600958013526));
#34112=CARTESIAN_POINT('Ctrl Pts',(85.4020134367339,-1.60964830794808,339.649410374396));
#34113=CARTESIAN_POINT('Ctrl Pts',(85.3942397663292,-1.47948403897286,339.692443117431));
#34114=CARTESIAN_POINT('Ctrl Pts',(85.3864660959246,-1.34792859282739,339.729933569421));
#34115=CARTESIAN_POINT('Ctrl Pts',(85.3790542917474,-1.22249708434969,339.765678831852));
#34116=CARTESIAN_POINT('Ctrl Pts',(85.3716424875703,-1.09580128225935,339.796386110771));
#34117=CARTESIAN_POINT('Ctrl Pts',(85.3642306833932,-0.968281059423146,
339.821992829989));
#34118=CARTESIAN_POINT('Ctrl Pts',(85.3564556046148,-0.834510690603265,
339.848854610793));
#34119=CARTESIAN_POINT('Ctrl Pts',(85.3486805258364,-0.699410303925138,
339.87018809065));
#34120=CARTESIAN_POINT('Ctrl Pts',(85.3409054470579,-0.563476562020997,
339.885865043833));
#34121=CARTESIAN_POINT('Ctrl Pts',(85.3331399360089,-0.427710095240234,
339.901522705527));
#34122=CARTESIAN_POINT('Ctrl Pts',(85.3253744249599,-0.291112698266287,
339.911537646023));
#34123=CARTESIAN_POINT('Ctrl Pts',(85.3176089139109,-0.15419248656926,339.915832354707));
#34124=CARTESIAN_POINT('Ctrl Pts',(85.3098511023887,-0.0174080316606694,
339.920122805175));
#34125=CARTESIAN_POINT('Ctrl Pts',(85.3020932908665,0.11969821284467,339.918704298513));
#34126=CARTESIAN_POINT('Ctrl Pts',(85.2943354793443,0.256612077399884,339.911551008005));
#34127=CARTESIAN_POINT('Ctrl Pts',(85.2865835058213,0.393422909930045,339.904403100574));
#34128=CARTESIAN_POINT('Ctrl Pts',(85.2788315322983,0.530041261901512,339.891529019612));
#34129=CARTESIAN_POINT('Ctrl Pts',(85.2710795587753,0.665952381888176,339.872955005698));
#34130=CARTESIAN_POINT('Ctrl Pts',(85.2633308682177,0.801805943434835,339.85438885789));
#34131=CARTESIAN_POINT('Ctrl Pts',(85.25558217766,0.936952482238757,339.830127631071));
#34132=CARTESIAN_POINT('Ctrl Pts',(85.2478334871024,1.07088200929846,339.800249450254));
#34133=CARTESIAN_POINT('Ctrl Pts',(85.2400864087246,1.20478367120145,339.770377485842));
#34134=CARTESIAN_POINT('Ctrl Pts',(85.2323393303467,1.33746844375498,339.734890977021));
#34135=CARTESIAN_POINT('Ctrl Pts',(85.2245922519689,1.46843657042959,339.693919162185));
#34136=CARTESIAN_POINT('Ctrl Pts',(85.2168451086631,1.59940579474326,339.652947003965));
#34137=CARTESIAN_POINT('Ctrl Pts',(85.2090979653573,1.72865797143602,339.606489564738));
#34138=CARTESIAN_POINT('Ctrl Pts',(85.2013508220515,1.85570892977093,339.55472583483));
#34139=CARTESIAN_POINT('Ctrl Pts',(85.1936019370234,1.98278845185855,339.502950467337));
#34140=CARTESIAN_POINT('Ctrl Pts',(85.1858530519953,2.10766540891845,339.445866582745));
#34141=CARTESIAN_POINT('Ctrl Pts',(85.1781041669672,2.2298763896427,339.383700987683));
#34142=CARTESIAN_POINT('Ctrl Pts',(85.1703470571925,2.35221708636465,339.321469409416));
#34143=CARTESIAN_POINT('Ctrl Pts',(85.1625899474177,2.47188580522838,339.254145523596));
#34144=CARTESIAN_POINT('Ctrl Pts',(85.154832837643,2.58844402060358,339.182001986454));
#34145=CARTESIAN_POINT('Ctrl Pts',(85.1470715827168,2.70506452096226,339.109819898111));
#34146=CARTESIAN_POINT('Ctrl Pts',(85.1393103277907,2.81857088254616,339.032813245931));
#34147=CARTESIAN_POINT('Ctrl Pts',(85.1315490728645,2.92855512860855,338.95129699228));
#34148=CARTESIAN_POINT('Ctrl Pts',(85.1237754024598,3.03871531362078,338.869650339189));
#34149=CARTESIAN_POINT('Ctrl Pts',(85.1160017320552,3.14534182006872,338.78347991495));
#34150=CARTESIAN_POINT('Ctrl Pts',(85.1082280616505,3.24806054153025,338.693140368447));
#34151=CARTESIAN_POINT('Ctrl Pts',(85.1008162574734,3.34599768179499,338.607006149569));
#34152=CARTESIAN_POINT('Ctrl Pts',(85.0934044532964,3.4403824560634,338.517082417262));
#34153=CARTESIAN_POINT('Ctrl Pts',(85.0859926491193,3.53092420223363,338.423705206437));
#34154=CARTESIAN_POINT('Ctrl Pts',(85.0782175703408,3.62590366909374,338.325751300352));
#34155=CARTESIAN_POINT('Ctrl Pts',(85.0704424915624,3.7169540187255,338.22368727302));
#34156=CARTESIAN_POINT('Ctrl Pts',(85.062667412784,3.80369865073104,338.117861388344));
#34157=CARTESIAN_POINT('Ctrl Pts',(85.054901901735,3.89033653794447,338.012165729157));
#34158=CARTESIAN_POINT('Ctrl Pts',(85.0471363906859,3.9726790045262,337.902717722823));
#34159=CARTESIAN_POINT('Ctrl Pts',(85.0393708796369,4.05038589971157,337.789902709042));
#34160=CARTESIAN_POINT('Ctrl Pts',(85.0316130681147,4.12801574828413,337.677199551675));
#34161=CARTESIAN_POINT('Ctrl Pts',(85.0238552565926,4.2010189518263,337.561136350288));
#34162=CARTESIAN_POINT('Ctrl Pts',(85.0160974450704,4.26909554545549,337.442131504705));
#34163=CARTESIAN_POINT('Ctrl Pts',(85.0083454715473,4.33712090928914,337.323216214042));
#34164=CARTESIAN_POINT('Ctrl Pts',(85.0005934980243,4.40022684936324,337.201364023321));
#34165=CARTESIAN_POINT('Ctrl Pts',(84.9928415245013,4.45815687040664,337.077021998282));
#34166=CARTESIAN_POINT('Ctrl Pts',(84.9850928339437,4.51606235805169,336.952732632164));
#34167=CARTESIAN_POINT('Ctrl Pts',(84.9773441433861,4.56879612168285,336.825955882518));
#34168=CARTESIAN_POINT('Ctrl Pts',(84.9695954528285,4.61614787397732,336.697162887903));
#34169=CARTESIAN_POINT('Ctrl Pts',(84.9618483744506,4.66348977434427,336.568396689745));
#34170=CARTESIAN_POINT('Ctrl Pts',(84.9541012960727,4.70545175588497,336.437615447661));
#34171=CARTESIAN_POINT('Ctrl Pts',(84.9463542176949,4.74187205098695,336.305309355888));
#34172=CARTESIAN_POINT('Ctrl Pts',(84.9386070743891,4.77829265132606,336.173002155262));
#34173=CARTESIAN_POINT('Ctrl Pts',(84.9308599310833,4.80917136885059,336.039170456314));
#34174=CARTESIAN_POINT('Ctrl Pts',(84.9231127877775,4.83439670777787,335.904318270481));
#34175=CARTESIAN_POINT('Ctrl Pts',(84.9153639027494,4.85962771789688,335.769435767015));
#34176=CARTESIAN_POINT('Ctrl Pts',(84.9076150177213,4.87920274841558,335.633532704265));
#34177=CARTESIAN_POINT('Ctrl Pts',(84.8998661326932,4.89306174741782,335.497121512768));
#34178=CARTESIAN_POINT('Ctrl Pts',(84.8921090229185,4.90693545650481,335.360565533023));
#34179=CARTESIAN_POINT('Ctrl Pts',(84.8843519131438,4.91508097499322,335.223500736649));
#34180=CARTESIAN_POINT('Ctrl Pts',(84.876594803369,4.91749027394364,335.086443439136));
#34181=CARTESIAN_POINT('Ctrl Pts',(84.8688335484429,4.91990086034638,334.949312902586));
#34182=CARTESIAN_POINT('Ctrl Pts',(84.8610722935167,4.91656912890944,334.812190263442));
#34183=CARTESIAN_POINT('Ctrl Pts',(84.8533110385905,4.90753915858057,334.675589042265));
#34184=CARTESIAN_POINT('Ctrl Pts',(84.8455373681859,4.89849474324204,334.538769303653));
#34185=CARTESIAN_POINT('Ctrl Pts',(84.8377636977812,4.88373391600003,334.40247303859));
#34186=CARTESIAN_POINT('Ctrl Pts',(84.8299900273765,4.86335245821817,334.26720676201));
#34187=CARTESIAN_POINT('Ctrl Pts',(84.8225782231995,4.8439197621996,334.138237163149));
#34188=CARTESIAN_POINT('Ctrl Pts',(84.8151664190224,4.81937799441778,334.010204101482));
#34189=CARTESIAN_POINT('Ctrl Pts',(84.8077546148453,4.78985243985645,333.883533848744));
#34190=CARTESIAN_POINT('Ctrl Pts',(84.7999795360669,4.75887974991389,333.750655109587));
#34191=CARTESIAN_POINT('Ctrl Pts',(84.7922044572885,4.72232450054317,333.618856226485));
#34192=CARTESIAN_POINT('Ctrl Pts',(84.78442937851,4.68027575420729,333.48864235633));
#34193=CARTESIAN_POINT('Ctrl Pts',(84.776663867461,4.63827875153073,333.358588722632));
#34194=CARTESIAN_POINT('Ctrl Pts',(84.768898356412,4.590801821511,333.230116589432));
#34195=CARTESIAN_POINT('Ctrl Pts',(84.761132845363,4.53798492942499,333.103720526185));
#34196=CARTESIAN_POINT('Ctrl Pts',(84.7533750338408,4.4852204054413,332.977449785003));
#34197=CARTESIAN_POINT('Ctrl Pts',(84.7456172223186,4.4271266056553,332.853251375715));
#34198=CARTESIAN_POINT('Ctrl Pts',(84.7378594107964,4.36389304319397,332.73160396534));
#34199=CARTESIAN_POINT('Ctrl Pts',(84.7301074372734,4.30070706599365,332.610048098499));
#34200=CARTESIAN_POINT('Ctrl Pts',(84.7223554637504,4.2323892044065,332.491039754908));
#34201=CARTESIAN_POINT('Ctrl Pts',(84.7146034902274,4.15917660124078,332.375036559837));
#34202=CARTESIAN_POINT('Ctrl Pts',(84.7068547996698,4.08599500365597,332.259082492188));
#34203=CARTESIAN_POINT('Ctrl Pts',(84.6991061091121,4.00792299557914,332.146131371644));
#34204=CARTESIAN_POINT('Ctrl Pts',(84.6913574185545,3.92524296893848,332.036614993407));
#34205=CARTESIAN_POINT('Ctrl Pts',(84.6836103401767,3.84258014456792,331.927121400968));
#34206=CARTESIAN_POINT('Ctrl Pts',(84.6758632617989,3.75531144399371,331.821061441153));
#34207=CARTESIAN_POINT('Ctrl Pts',(84.668116183421,3.66376154027064,331.718836420028));
#34208=CARTESIAN_POINT('Ctrl Pts',(84.6603690401152,3.57221086927126,331.616610542159));
#34209=CARTESIAN_POINT('Ctrl Pts',(84.6526218968095,3.47637918432452,331.518219958262));
#34210=CARTESIAN_POINT('Ctrl Pts',(84.6448747535037,3.37662998263609,331.424031177029));
#34211=CARTESIAN_POINT('Ctrl Pts',(84.6371258684756,3.27685835520939,331.329821220157));
#34212=CARTESIAN_POINT('Ctrl Pts',(84.6293769834474,3.17316774260688,331.239815214009));
#34213=CARTESIAN_POINT('Ctrl Pts',(84.6216280984194,3.06595656106129,331.154340963088));
#34214=CARTESIAN_POINT('Ctrl Pts',(84.6138709886446,2.95863158445983,331.068775988913));
#34215=CARTESIAN_POINT('Ctrl Pts',(84.6061138788699,2.84777888048379,330.987752622545));
#34216=CARTESIAN_POINT('Ctrl Pts',(84.5983567690952,2.73382828492385,330.911557023627));
#34217=CARTESIAN_POINT('Ctrl Pts',(84.590595514169,2.61981679780916,330.835320708218));
#34218=CARTESIAN_POINT('Ctrl Pts',(84.5828342592429,2.50270445411489,330.763917504127));
#34219=CARTESIAN_POINT('Ctrl Pts',(84.5750730043167,2.38294693788354,330.697588239867));
#34220=CARTESIAN_POINT('Ctrl Pts',(84.567299333912,2.2629978486551,330.631152870401));
#34221=CARTESIAN_POINT('Ctrl Pts',(84.5595256635074,2.14039548101372,330.569807835234));
#34222=CARTESIAN_POINT('Ctrl Pts',(84.5517519931027,2.01561760696511,330.513746694067));
#34223=CARTESIAN_POINT('Ctrl Pts',(84.5443401889256,1.89664817297303,330.46029521251));
#34224=CARTESIAN_POINT('Ctrl Pts',(84.5369283847485,1.77570148119809,330.411646872409));
#34225=CARTESIAN_POINT('Ctrl Pts',(84.5295165805714,1.65320379152928,330.367926999045));
#34226=CARTESIAN_POINT('Ctrl Pts',(84.521741501793,1.52470212518811,330.322064284453));
#34227=CARTESIAN_POINT('Ctrl Pts',(84.5139664230146,1.39408748960774,330.281480435256));
#34228=CARTESIAN_POINT('Ctrl Pts',(84.5061913442361,1.26183287880432,330.24637392631));
#34229=CARTESIAN_POINT('Ctrl Pts',(84.4984258331871,1.12974101571923,330.211310618157));
#34230=CARTESIAN_POINT('Ctrl Pts',(84.4906603221381,0.99601356701873,330.181711338482));
#34231=CARTESIAN_POINT('Ctrl Pts',(84.482894811089,0.861142169952539,330.157726027409));
#34232=CARTESIAN_POINT('Ctrl Pts',(84.4751369995668,0.726404498269299,330.133764497842));
#34233=CARTESIAN_POINT('Ctrl Pts',(84.4673791880446,0.590525517755629,330.115405927689));
#34234=CARTESIAN_POINT('Ctrl Pts',(84.4596213765224,0.454010306148653,330.102749985511));
#34235=CARTESIAN_POINT('Ctrl Pts',(84.4518694029994,0.317597826567557,330.090103567331));
#34236=CARTESIAN_POINT('Ctrl Pts',(84.4441174294764,0.180550456527649,330.083151271223));
#34237=CARTESIAN_POINT('Ctrl Pts',(84.4363654559534,0.0433813544616911,
330.081941326033));
#34238=CARTESIAN_POINT('Ctrl Pts',(84.4286167653958,-0.093729656408104,
330.080731893255));
#34239=CARTESIAN_POINT('Ctrl Pts',(84.4208680748382,-0.23096190672186,330.085259977979));
#34240=CARTESIAN_POINT('Ctrl Pts',(84.4131193842805,-0.367799472204802,
330.09552177997));
#34241=CARTESIAN_POINT('Ctrl Pts',(84.4053723059027,-0.504608567489355,
330.105781446908));
#34242=CARTESIAN_POINT('Ctrl Pts',(84.3976252275249,-0.641022751745491,
330.121772429041));
#34243=CARTESIAN_POINT('Ctrl Pts',(84.389878149147,-0.776528858921388,330.143438871613));
#34244=CARTESIAN_POINT('Ctrl Pts',(84.3821310058412,-0.91203610176898,330.16510549577));
#34245=CARTESIAN_POINT('Ctrl Pts',(84.3743838625354,-1.04663486638488,330.192447613524));
#34246=CARTESIAN_POINT('Ctrl Pts',(84.3666367192296,-1.17982023859552,330.225357891203));
#34247=CARTESIAN_POINT('Ctrl Pts',(84.3588878342015,-1.31303555370516,330.258275567811));
#34248=CARTESIAN_POINT('Ctrl Pts',(84.3511389491734,-1.4448364647144,330.29676380162));
#34249=CARTESIAN_POINT('Ctrl Pts',(84.3433900641453,-1.5747317079378,330.340664949747));
#34250=CARTESIAN_POINT('Ctrl Pts',(84.3356329543706,-1.70476482331461,330.384612695006));
#34251=CARTESIAN_POINT('Ctrl Pts',(84.3278758445958,-1.83288785949952,330.433984706057));
#34252=CARTESIAN_POINT('Ctrl Pts',(84.3201187348211,-1.9586275699325,330.488574382216));
#34253=CARTESIAN_POINT('Ctrl Pts',(84.3123574798949,-2.08443447164635,330.543193229352));
#34254=CARTESIAN_POINT('Ctrl Pts',(84.3045962249688,-2.20785515836516,330.603035126798));
#34255=CARTESIAN_POINT('Ctrl Pts',(84.2968349700426,-2.32844051547162,330.667847206248));
#34256=CARTESIAN_POINT('Ctrl Pts',(84.289061299638,-2.44921876985078,330.732762963903));
#34257=CARTESIAN_POINT('Ctrl Pts',(84.2812876292333,-2.5671522947151,330.802664591954));
#34258=CARTESIAN_POINT('Ctrl Pts',(84.2735139588286,-2.68181977173455,330.877255067988));
#34259=CARTESIAN_POINT('Ctrl Pts',(84.2661021546516,-2.79114945011089,330.948373339417));
#34260=CARTESIAN_POINT('Ctrl Pts',(84.2586903504745,-2.89751007200662,331.023753584545));
#34261=CARTESIAN_POINT('Ctrl Pts',(84.2512785462974,-3.00056557503607,331.103105173037));
#34262=CARTESIAN_POINT('Ctrl Pts',(84.2435911514805,-3.10745295642346,331.185407265149));
#34263=CARTESIAN_POINT('Ctrl Pts',(84.2359037566636,-3.21113912003713,331.272254895859));
#34264=CARTESIAN_POINT('Ctrl Pts',(84.2282163618467,-3.31120629745287,331.363367503004));
#34265=CARTESIAN_POINT('Ctrl Pts',(84.2205384662962,-3.41114982247456,331.454367522862));
#34266=CARTESIAN_POINT('Ctrl Pts',(84.2128605707456,-3.50748296219958,331.549621770662));
#34267=CARTESIAN_POINT('Ctrl Pts',(84.2051826751951,-3.59981823082209,331.648807411153));
#34268=CARTESIAN_POINT('Ctrl Pts',(84.1975123291306,-3.69206270844377,331.747895524842));
#34269=CARTESIAN_POINT('Ctrl Pts',(84.1898419830661,-3.78031686356381,331.850907050325));
#34270=CARTESIAN_POINT('Ctrl Pts',(84.1821716370016,-3.86422790263018,331.957480356837));
#34271=CARTESIAN_POINT('Ctrl Pts',(84.1744368291485,-3.94884413226014,332.0649493082));
#34272=CARTESIAN_POINT('Ctrl Pts',(84.1667020212954,-4.02904359458647,332.176039916274));
#34273=CARTESIAN_POINT('Ctrl Pts',(84.1589672134423,-4.10450368599915,332.290344569116));
#34274=CARTESIAN_POINT('Ctrl Pts',(84.151305538029,-4.17925030389098,332.403568473955));
#34275=CARTESIAN_POINT('Ctrl Pts',(84.1436438626156,-4.2493465680269,332.519945562008));
#34276=CARTESIAN_POINT('Ctrl Pts',(84.1359821872023,-4.31452095120334,332.639048491788));
#34277=CARTESIAN_POINT('Ctrl Pts',(84.1283217735525,-4.37968460113241,332.758131807095));
#34278=CARTESIAN_POINT('Ctrl Pts',(84.1206613599026,-4.43992778997178,332.879939720091));
#34279=CARTESIAN_POINT('Ctrl Pts',(84.1130009462528,-4.4950242715391,333.004019073043));
#34280=CARTESIAN_POINT('Ctrl Pts',(84.1053400457857,-4.55012425447306,333.128106311205));
#34281=CARTESIAN_POINT('Ctrl Pts',(84.0976791453187,-4.60007671776464,333.254464910044));
#34282=CARTESIAN_POINT('Ctrl Pts',(84.0900182448516,-4.64470322883895,333.382620953977));
#34283=CARTESIAN_POINT('Ctrl Pts',(84.0822280784912,-4.69008274353803,333.51293943372));
#34284=CARTESIAN_POINT('Ctrl Pts',(84.0744379121308,-4.7299547920782,333.645116164544));
#34285=CARTESIAN_POINT('Ctrl Pts',(84.0666477457704,-4.76418464552896,333.778636939397));
#34286=CARTESIAN_POINT('Ctrl Pts',(84.0589769385894,-4.79789003685257,333.910111938924));
#34287=CARTESIAN_POINT('Ctrl Pts',(84.0513061314085,-4.8261248771364,334.042889681328));
#34288=CARTESIAN_POINT('Ctrl Pts',(84.0436353242275,-4.84881237358444,334.176470019808));
#34289=CARTESIAN_POINT('Ctrl Pts',(84.0357854782774,-4.87202940249804,334.313168160473));
#34290=CARTESIAN_POINT('Ctrl Pts',(84.0279356323272,-4.88943688677875,334.450706378763));
#34291=CARTESIAN_POINT('Ctrl Pts',(84.0200857863771,-4.9010088882587,334.588545336994));
#34292=CARTESIAN_POINT('Ctrl Pts',(84.012235940427,-4.91258088973864,334.726384295226));
#34293=CARTESIAN_POINT('Ctrl Pts',(84.0043860944769,-4.9183174533213,334.864523548469));
#34294=CARTESIAN_POINT('Ctrl Pts',(83.9965362485268,-4.91824940115574,335.002427041656));
#34295=CARTESIAN_POINT('',(87.4965362485424,-4.91824854721736,334.996219749433));
#34296=CARTESIAN_POINT('Ctrl Pts',(87.4965362484899,-4.91824854721807,334.996219750363));
#34297=CARTESIAN_POINT('Ctrl Pts',(87.4887898181956,-4.9183540119818,335.133433418973));
#34298=CARTESIAN_POINT('Ctrl Pts',(87.4810433879014,-4.9127130140224,335.27071194917));
#34299=CARTESIAN_POINT('Ctrl Pts',(87.4732969576071,-4.90133605169373,335.407538919451));
#34300=CARTESIAN_POINT('Ctrl Pts',(87.4655516439243,-4.88996072930072,335.544346166768));
#34301=CARTESIAN_POINT('Ctrl Pts',(87.4578063302416,-4.8728511191656,335.68070159468));
#34302=CARTESIAN_POINT('Ctrl Pts',(87.4500610165588,-4.85006973752551,335.816092276424));
#34303=CARTESIAN_POINT('Ctrl Pts',(87.4423151479825,-4.82728672377053,335.951492657894));
#34304=CARTESIAN_POINT('Ctrl Pts',(87.4345692794062,-4.79883119428449,336.085927770556));
#34305=CARTESIAN_POINT('Ctrl Pts',(87.4268234108299,-4.76481702747752,336.218893661137));
#34306=CARTESIAN_POINT('Ctrl Pts',(87.4190753158446,-4.73079308391719,336.351897770345));
#34307=CARTESIAN_POINT('Ctrl Pts',(87.4113272208593,-4.69120742003832,336.483431438911));
#34308=CARTESIAN_POINT('Ctrl Pts',(87.403579125874,-4.64622402945685,336.613005062174));
#34309=CARTESIAN_POINT('Ctrl Pts',(87.3958220968729,-4.60118877034202,336.742728091555));
#34310=CARTESIAN_POINT('Ctrl Pts',(87.3880650678718,-4.55074348051424,336.870486191809));
#34311=CARTESIAN_POINT('Ctrl Pts',(87.3803080388706,-4.49510087465192,336.995808404934));
#34312=CARTESIAN_POINT('Ctrl Pts',(87.372546455652,-4.43942560054399,337.121204195792));
#34313=CARTESIAN_POINT('Ctrl Pts',(87.3647848724334,-4.37854710396342,337.244160900628));
#34314=CARTESIAN_POINT('Ctrl Pts',(87.3570232892148,-4.31272402621819,337.364232335491));
#34315=CARTESIAN_POINT('Ctrl Pts',(87.3492487195698,-4.24679081545928,337.484504669938));
#34316=CARTESIAN_POINT('Ctrl Pts',(87.3414741499249,-4.17589669410478,337.601881753829));
#34317=CARTESIAN_POINT('Ctrl Pts',(87.33369958028,-4.10034408335858,337.715945776441));
#34318=CARTESIAN_POINT('Ctrl Pts',(87.3264320279569,-4.02971862409632,337.822571131973));
#34319=CARTESIAN_POINT('Ctrl Pts',(87.3191644756338,-3.95502304272049,337.926301559397));
#34320=CARTESIAN_POINT('Ctrl Pts',(87.3118969233108,-3.87653494268447,338.026823400968));
#34321=CARTESIAN_POINT('Ctrl Pts',(87.3041218445323,-3.79256565924173,338.134365143005));
#34322=CARTESIAN_POINT('Ctrl Pts',(87.2963467657539,-3.70398520819931,338.238579995768));
#34323=CARTESIAN_POINT('Ctrl Pts',(87.2885716869754,-3.6110867843188,338.339047064451));
#34324=CARTESIAN_POINT('Ctrl Pts',(87.2808061759264,-3.51830267786327,338.439390502009));
#34325=CARTESIAN_POINT('Ctrl Pts',(87.2730406648774,-3.42121143382314,338.535995047575));
#34326=CARTESIAN_POINT('Ctrl Pts',(87.2652751538284,-3.32014798085434,338.628470813956));
#34327=CARTESIAN_POINT('Ctrl Pts',(87.2575173423062,-3.21918473259312,338.720854890346));
#34328=CARTESIAN_POINT('Ctrl Pts',(87.249759530784,-3.1142573996672,338.809118072073));
#34329=CARTESIAN_POINT('Ctrl Pts',(87.2420017192618,-3.0057391806178,338.892905732303));
#34330=CARTESIAN_POINT('Ctrl Pts',(87.2342497457388,-2.89730262496962,338.976630339662));
#34331=CARTESIAN_POINT('Ctrl Pts',(87.2264977722158,-2.78528087004586,339.055885891391));
#34332=CARTESIAN_POINT('Ctrl Pts',(87.2187457986928,-2.67008148311988,339.130356877559));
#34333=CARTESIAN_POINT('Ctrl Pts',(87.2109971081352,-2.55493088320274,339.20479632522));
#34334=CARTESIAN_POINT('Ctrl Pts',(87.2032484175775,-2.43660565541755,339.274455025661));
#34335=CARTESIAN_POINT('Ctrl Pts',(87.1954997270199,-2.31554356265198,339.339059929519));
#34336=CARTESIAN_POINT('Ctrl Pts',(87.1877526486421,-2.1945066578662,339.403651391788));
#34337=CARTESIAN_POINT('Ctrl Pts',(87.1800055702643,-2.07073436535895,339.463190965043));
#34338=CARTESIAN_POINT('Ctrl Pts',(87.1722584918865,-1.94468999186234,339.517451039917));
#34339=CARTESIAN_POINT('Ctrl Pts',(87.1645113485807,-1.81864456199213,339.571711569544));
#34340=CARTESIAN_POINT('Ctrl Pts',(87.1567642052748,-1.69032737217248,339.620692357984));
#34341=CARTESIAN_POINT('Ctrl Pts',(87.149017061969,-1.5602223250501,339.664213691386));
#34342=CARTESIAN_POINT('Ctrl Pts',(87.1412681769409,-1.43008802755092,339.707744809308));
#34343=CARTESIAN_POINT('Ctrl Pts',(87.1335192919128,-1.29816544352934,339.745813905828));
#34344=CARTESIAN_POINT('Ctrl Pts',(87.1257704068847,-1.16495388577462,339.778291065488));
#34345=CARTESIAN_POINT('Ctrl Pts',(87.11801329711,-1.03160093589634,339.810802696741));
#34346=CARTESIAN_POINT('Ctrl Pts',(87.1102561873352,-0.896956659667793,
339.837710442007));
#34347=CARTESIAN_POINT('Ctrl Pts',(87.1024990775605,-0.761531368509716,
339.858935381056));
#34348=CARTESIAN_POINT('Ctrl Pts',(87.0947378226343,-0.626033710406198,
339.880171662034));
#34349=CARTESIAN_POINT('Ctrl Pts',(87.0869765677082,-0.489754593925044,
339.895719041593));
#34350=CARTESIAN_POINT('Ctrl Pts',(87.079215312782,-0.353208724307071,339.905550596984));
#34351=CARTESIAN_POINT('Ctrl Pts',(87.0714416423774,-0.216444425797904,
339.91539787966));
#34352=CARTESIAN_POINT('Ctrl Pts',(87.0636679719727,-0.0794129123466384,
339.9195110551));
#34353=CARTESIAN_POINT('Ctrl Pts',(87.055894301568,0.0573709434497541,339.917915375171));
#34354=CARTESIAN_POINT('Ctrl Pts',(87.048482497391,0.187787477849971,339.916393974527));
#34355=CARTESIAN_POINT('Ctrl Pts',(87.0410706932139,0.317978605226491,339.909683266813));
#34356=CARTESIAN_POINT('Ctrl Pts',(87.0336588890369,0.447504879302989,339.897848756903));
#34357=CARTESIAN_POINT('Ctrl Pts',(87.0258838102584,0.583379621911605,339.88543420241));
#34358=CARTESIAN_POINT('Ctrl Pts',(87.01810873148,0.71895207973114,339.867341648025));
#34359=CARTESIAN_POINT('Ctrl Pts',(87.0103336527016,0.853709648829552,339.843589877146));
#34360=CARTESIAN_POINT('Ctrl Pts',(87.0025681416526,0.988301390159919,339.819867334334));
#34361=CARTESIAN_POINT('Ctrl Pts',(86.9948026306035,1.12207985673796,339.790499498643));
#34362=CARTESIAN_POINT('Ctrl Pts',(86.9870371195545,1.25453593499316,339.755557028394));
#34363=CARTESIAN_POINT('Ctrl Pts',(86.9792793080324,1.38686068266104,339.720649203707));
#34364=CARTESIAN_POINT('Ctrl Pts',(86.9715214965101,1.51786527576267,339.680177843096));
#34365=CARTESIAN_POINT('Ctrl Pts',(86.963763684988,1.64704954188327,339.634264868248));
#34366=CARTESIAN_POINT('Ctrl Pts',(86.956011711465,1.77613659274712,339.58838644437));
#34367=CARTESIAN_POINT('Ctrl Pts',(86.9482597379419,1.90340567643511,339.537074687499));
#34368=CARTESIAN_POINT('Ctrl Pts',(86.9405077644189,2.02837091587768,339.480501589122));
#34369=CARTESIAN_POINT('Ctrl Pts',(86.9327590738613,2.15328323246706,339.423952449485));
#34370=CARTESIAN_POINT('Ctrl Pts',(86.9250103833037,2.27589329002514,339.362146560906));
#34371=CARTESIAN_POINT('Ctrl Pts',(86.9172616927461,2.39573457690208,339.29530428486));
#34372=CARTESIAN_POINT('Ctrl Pts',(86.9095146143682,2.51555092979835,339.228475915907));
#34373=CARTESIAN_POINT('Ctrl Pts',(86.9017675359904,2.63259931669743,339.15661343404));
#34374=CARTESIAN_POINT('Ctrl Pts',(86.8940204576126,2.74643761417148,339.079983271285));
#34375=CARTESIAN_POINT('Ctrl Pts',(86.8862733143068,2.86027686572018,339.003352466295));
#34376=CARTESIAN_POINT('Ctrl Pts',(86.8785261710009,2.97090564992886,338.921954118991));
#34377=CARTESIAN_POINT('Ctrl Pts',(86.8707790276951,3.07791097409765,338.836097899954));
#34378=CARTESIAN_POINT('Ctrl Pts',(86.863030142667,3.18494035533518,338.750222378616));
#34379=CARTESIAN_POINT('Ctrl Pts',(86.8552812576389,3.28834435069716,338.659887235798));
#34380=CARTESIAN_POINT('Ctrl Pts',(86.8475323726108,3.38774350470389,338.565442049569));
#34381=CARTESIAN_POINT('Ctrl Pts',(86.8397752628361,3.48724816199954,338.470896618244));
#34382=CARTESIAN_POINT('Ctrl Pts',(86.8320181530613,3.58273920279971,338.372232698784));
#34383=CARTESIAN_POINT('Ctrl Pts',(86.8242610432866,3.67387410260758,338.269836714683));
#34384=CARTESIAN_POINT('Ctrl Pts',(86.8164997883604,3.76505770199198,338.167386013443));
#34385=CARTESIAN_POINT('Ctrl Pts',(86.8087385334343,3.8518802747747,338.061199576194));
#34386=CARTESIAN_POINT('Ctrl Pts',(86.8009772785081,3.93404064450069,337.951695660111));
#34387=CARTESIAN_POINT('Ctrl Pts',(86.7932036081034,4.01633244404224,337.842016573449));
#34388=CARTESIAN_POINT('Ctrl Pts',(86.7854299376988,4.09394691581605,337.729009725593));
#34389=CARTESIAN_POINT('Ctrl Pts',(86.7776562672941,4.16662666754909,337.613121749129));
#34390=CARTESIAN_POINT('Ctrl Pts',(86.7702444631171,4.23592315935297,337.50262838585));
#34391=CARTESIAN_POINT('Ctrl Pts',(86.76283265894,4.3007338714579,337.389516340328));
#34392=CARTESIAN_POINT('Ctrl Pts',(86.7554208547629,4.36087607871603,337.274190600759));
#34393=CARTESIAN_POINT('Ctrl Pts',(86.7476457759845,4.4239660347065,337.153212403156));
#34394=CARTESIAN_POINT('Ctrl Pts',(86.739870697206,4.48211765580835,337.029415711736));
#34395=CARTESIAN_POINT('Ctrl Pts',(86.7320956184276,4.53506933798152,336.903241750856));
#34396=CARTESIAN_POINT('Ctrl Pts',(86.7243301073786,4.58795585973866,336.777223055067));
#34397=CARTESIAN_POINT('Ctrl Pts',(86.7165645963296,4.63565502464282,336.648833267464));
#34398=CARTESIAN_POINT('Ctrl Pts',(86.7087990852806,4.67795074021808,336.518538749783));
#34399=CARTESIAN_POINT('Ctrl Pts',(86.7010412737584,4.72020451946815,336.388373419496));
#34400=CARTESIAN_POINT('Ctrl Pts',(86.6932834622363,4.75706539128104,336.256307486823));
#34401=CARTESIAN_POINT('Ctrl Pts',(86.6855256507141,4.78836521021092,336.122827536241));
#34402=CARTESIAN_POINT('Ctrl Pts',(86.6777736771911,4.8196414750345,335.989448033555));
#34403=CARTESIAN_POINT('Ctrl Pts',(86.670021703668,4.84536492787493,335.854657010004));
#34404=CARTESIAN_POINT('Ctrl Pts',(86.662269730145,4.86541726408165,335.718956124445));
#34405=CARTESIAN_POINT('Ctrl Pts',(86.6545210395874,4.88546110811208,335.583312708291));
#34406=CARTESIAN_POINT('Ctrl Pts',(86.6467723490298,4.89983855534358,335.446760582388));
#34407=CARTESIAN_POINT('Ctrl Pts',(86.6390236584722,4.90848245621954,335.309811296574));
#34408=CARTESIAN_POINT('Ctrl Pts',(86.6312765800944,4.91712455865974,335.172890504203));
#34409=CARTESIAN_POINT('Ctrl Pts',(86.6235295017166,4.92003546292459,335.035573106135));
#34410=CARTESIAN_POINT('Ctrl Pts',(86.6157824233388,4.91719995903452,334.898375075051));
#34411=CARTESIAN_POINT('Ctrl Pts',(86.608035280033,4.9143644313802,334.761175894115));
#34412=CARTESIAN_POINT('Ctrl Pts',(86.6002881367271,4.90578240758793,334.62409647295));
#34413=CARTESIAN_POINT('Ctrl Pts',(86.5925409934213,4.8914908022096,334.487651686449));
#34414=CARTESIAN_POINT('Ctrl Pts',(86.5847921083932,4.87719598377492,334.351176224262));
#34415=CARTESIAN_POINT('Ctrl Pts',(86.5770432233652,4.85718907017415,334.215336069327));
#34416=CARTESIAN_POINT('Ctrl Pts',(86.569294338337,4.83155868393009,334.080639490602));
#34417=CARTESIAN_POINT('Ctrl Pts',(86.5615372285623,4.80590109332929,333.945799943538));
#34418=CARTESIAN_POINT('Ctrl Pts',(86.5537801187876,4.77460818000428,333.812106781963));
#34419=CARTESIAN_POINT('Ctrl Pts',(86.5460230090128,4.73781953605724,333.680057157959));
#34420=CARTESIAN_POINT('Ctrl Pts',(86.5382617540867,4.70101123343516,333.547936970859));
#34421=CARTESIAN_POINT('Ctrl Pts',(86.5305004991605,4.6587014689758,333.417462442956));
#34422=CARTESIAN_POINT('Ctrl Pts',(86.5227392442344,4.61107898019732,333.289113182913));
#34423=CARTESIAN_POINT('Ctrl Pts',(86.5149655738297,4.56338031095693,333.160558605882));
#34424=CARTESIAN_POINT('Ctrl Pts',(86.507191903425,4.51035208589418,333.034136451029));
#34425=CARTESIAN_POINT('Ctrl Pts',(86.4994182330204,4.45223059814982,332.910304863527));
#34426=CARTESIAN_POINT('Ctrl Pts',(86.4920064288432,4.39681467964284,332.792237666214));
#34427=CARTESIAN_POINT('Ctrl Pts',(86.4845946246661,4.33676914258128,332.676525537529));
#34428=CARTESIAN_POINT('Ctrl Pts',(86.477182820489,4.27233566711696,332.563541297296));
#34429=CARTESIAN_POINT('Ctrl Pts',(86.4694077417106,4.2047441150831,332.445019362888));
#34430=CARTESIAN_POINT('Ctrl Pts',(86.4616326629321,4.13211001509869,332.329124930913));
#34431=CARTESIAN_POINT('Ctrl Pts',(86.4538575841537,4.05466283318189,332.216316761606));
#34432=CARTESIAN_POINT('Ctrl Pts',(86.4460920731047,3.97731095495308,332.103647409934));
#34433=CARTESIAN_POINT('Ctrl Pts',(86.4383265620557,3.89515799858936,331.994057083473));
#34434=CARTESIAN_POINT('Ctrl Pts',(86.4305610510067,3.80847919758504,331.887979874091));
#34435=CARTESIAN_POINT('Ctrl Pts',(86.4228032394845,3.72188633886409,331.782007840571));
#34436=CARTESIAN_POINT('Ctrl Pts',(86.4150454279623,3.63077681139094,331.67954229296));
#34437=CARTESIAN_POINT('Ctrl Pts',(86.4072876164401,3.5354688012825,331.580987947132));
#34438=CARTESIAN_POINT('Ctrl Pts',(86.3995356429171,3.44023251347452,331.482507766574));
#34439=CARTESIAN_POINT('Ctrl Pts',(86.3917836693941,3.34080430247368,331.387933209144));
#34440=CARTESIAN_POINT('Ctrl Pts',(86.3840316958711,3.23754200248008,331.297635236139));
#34441=CARTESIAN_POINT('Ctrl Pts',(86.3762830053135,3.13432343413148,331.207375504379));
#34442=CARTESIAN_POINT('Ctrl Pts',(86.3685343147559,3.02727429992282,331.121389011588));
#34443=CARTESIAN_POINT('Ctrl Pts',(86.3607856241982,2.91678843454769,331.040009054229));
#34444=CARTESIAN_POINT('Ctrl Pts',(86.3530385458204,2.80632555667973,330.95864602865));
#34445=CARTESIAN_POINT('Ctrl Pts',(86.3452914674426,2.69242768443144,330.881887863787));
#34446=CARTESIAN_POINT('Ctrl Pts',(86.3375443890648,2.57552047924526,330.81002657246));
#34447=CARTESIAN_POINT('Ctrl Pts',(86.329797245759,2.45861229426402,330.738164678867));
#34448=CARTESIAN_POINT('Ctrl Pts',(86.3220501024532,2.33869505903454,330.671199945355));
#34449=CARTESIAN_POINT('Ctrl Pts',(86.3143029591474,2.21622171942105,330.609379958039));
#34450=CARTESIAN_POINT('Ctrl Pts',(86.3065540741193,2.09372084520096,330.547546072278));
#34451=CARTESIAN_POINT('Ctrl Pts',(86.2988051890912,1.96866307194777,330.490859410412));
#34452=CARTESIAN_POINT('Ctrl Pts',(86.2910563040631,1.84152377260569,330.43952050137));
#34453=CARTESIAN_POINT('Ctrl Pts',(86.2832991942884,1.71424952629734,330.388127100678));
#34454=CARTESIAN_POINT('Ctrl Pts',(86.2755420845137,1.58488970352282,330.342092938058));
#34455=CARTESIAN_POINT('Ctrl Pts',(86.2677849747389,1.45393791137153,330.30156966505));
#34456=CARTESIAN_POINT('Ctrl Pts',(86.2600237198128,1.32291614276945,330.261024737701));
#34457=CARTESIAN_POINT('Ctrl Pts',(86.2522624648866,1.1903010874211,330.225996667599));
#34458=CARTESIAN_POINT('Ctrl Pts',(86.2445012099604,1.05659819518321,330.196586285106));
#34459=CARTESIAN_POINT('Ctrl Pts',(86.2367275395557,0.922681421891414,330.167128855585));
#34460=CARTESIAN_POINT('Ctrl Pts',(86.2289538691511,0.787673719436697,330.143307139255));
#34461=CARTESIAN_POINT('Ctrl Pts',(86.2211801987464,0.652088223646006,330.125170360814));
#34462=CARTESIAN_POINT('Ctrl Pts',(86.2137683945693,0.52281426530389,330.107877853773));
#34463=CARTESIAN_POINT('Ctrl Pts',(86.2063565903922,0.393015382166143,330.095752954512));
#34464=CARTESIAN_POINT('Ctrl Pts',(86.1989447862151,0.263135873376105,330.088794183233));
#34465=CARTESIAN_POINT('Ctrl Pts',(86.1911697074366,0.126890582969666,330.081494341846));
#34466=CARTESIAN_POINT('Ctrl Pts',(86.1833946286582,-0.0098739966229407,
330.07985677894));
#34467=CARTESIAN_POINT('Ctrl Pts',(86.1756195498798,-0.146647906903237,
330.083936793134));
#34468=CARTESIAN_POINT('Ctrl Pts',(86.1678540388307,-0.283253508179759,
330.088011786611));
#34469=CARTESIAN_POINT('Ctrl Pts',(86.1600885277817,-0.419868030332519,
330.097790346334));
#34470=CARTESIAN_POINT('Ctrl Pts',(86.1523230167327,-0.555977491612252,
330.113275934604));
#34471=CARTESIAN_POINT('Ctrl Pts',(86.1445652052104,-0.691951999965223,
330.128746168868));
#34472=CARTESIAN_POINT('Ctrl Pts',(86.1368073936882,-0.827422058137413,
330.149912126973));
#34473=CARTESIAN_POINT('Ctrl Pts',(86.129049582166,-0.961875143152225,330.176725254406));
#34474=CARTESIAN_POINT('Ctrl Pts',(86.121297608643,-1.09622704795599,330.20351820411));
#34475=CARTESIAN_POINT('Ctrl Pts',(86.1135456351199,-1.22956312112094,330.235949788236));
#34476=CARTESIAN_POINT('Ctrl Pts',(86.1057936615969,-1.36137776876012,330.273919844816));
#34477=CARTESIAN_POINT('Ctrl Pts',(86.0980449710393,-1.49313659281804,330.311873821054));
#34478=CARTESIAN_POINT('Ctrl Pts',(86.0902962804817,-1.62337489804639,330.35536149665));
#34479=CARTESIAN_POINT('Ctrl Pts',(86.082547589924,-1.75159928178674,330.404232053449));
#34480=CARTESIAN_POINT('Ctrl Pts',(86.0748005115462,-1.87979698737267,330.453092442321));
#34481=CARTESIAN_POINT('Ctrl Pts',(86.0670534331684,-2.00598123990152,330.507333345609));
#34482=CARTESIAN_POINT('Ctrl Pts',(86.0593063547906,-2.1296761297318,330.566754840419));
#34483=CARTESIAN_POINT('Ctrl Pts',(86.0515592114848,-2.25337205624465,330.626176833238));
#34484=CARTESIAN_POINT('Ctrl Pts',(86.043812068179,-2.37457822611672,330.690779334926));
#34485=CARTESIAN_POINT('Ctrl Pts',(86.0360649248732,-2.49284132390555,330.760315436695));
#34486=CARTESIAN_POINT('Ctrl Pts',(86.0283160398451,-2.61113100974916,330.829867171655));
#34487=CARTESIAN_POINT('Ctrl Pts',(86.020567154817,-2.72647596998999,330.904354515759));
#34488=CARTESIAN_POINT('Ctrl Pts',(86.0128182697889,-2.83845032399687,330.983486235465));
#34489=CARTESIAN_POINT('Ctrl Pts',(86.0050611600142,-2.9505435287403,331.062701946396));
#34490=CARTESIAN_POINT('Ctrl Pts',(85.9973040502395,-3.0592586609519,331.146571654304));
#34491=CARTESIAN_POINT('Ctrl Pts',(85.9895469404648,-3.16420107449538,331.234762341809));
#34492=CARTESIAN_POINT('Ctrl Pts',(85.9817856855386,-3.2691995659094,331.323000155597));
#34493=CARTESIAN_POINT('Ctrl Pts',(85.9740244306124,-3.37042103324849,331.415563286215));
#34494=CARTESIAN_POINT('Ctrl Pts',(85.9662631756862,-3.46750715819042,331.51208125519));
#34495=CARTESIAN_POINT('Ctrl Pts',(85.9584895052816,-3.5647485892919,331.608753621459));
#34496=CARTESIAN_POINT('Ctrl Pts',(85.9507158348769,-3.65784119330613,331.709393181121));
#34497=CARTESIAN_POINT('Ctrl Pts',(85.9429421644722,-3.74646588889447,331.813595065619));
#34498=CARTESIAN_POINT('Ctrl Pts',(85.9355303602952,-3.8309650835803,331.912946327322));
#34499=CARTESIAN_POINT('Ctrl Pts',(85.9281185561182,-3.91140279356588,332.015535498572));
#34500=CARTESIAN_POINT('Ctrl Pts',(85.9207067519412,-3.98753982748235,332.120988157936));
#34501=CARTESIAN_POINT('Ctrl Pts',(85.9128697277735,-4.06804489218859,332.232490704449));
#34502=CARTESIAN_POINT('Ctrl Pts',(85.9050327036058,-4.14399504332485,332.347546226307));
#34503=CARTESIAN_POINT('Ctrl Pts',(85.8971956794381,-4.21506351142011,332.465750079966));
#34504=CARTESIAN_POINT('Ctrl Pts',(85.8893685771602,-4.28604200486538,332.583804284269));
#34505=CARTESIAN_POINT('Ctrl Pts',(85.8815414748823,-4.35215091783572,332.70499856482));
#34506=CARTESIAN_POINT('Ctrl Pts',(85.8737143726044,-4.41310477941014,332.82889676237));
#34507=CARTESIAN_POINT('Ctrl Pts',(85.8658955767316,-4.47399395453352,332.952663474654));
#34508=CARTESIAN_POINT('Ctrl Pts',(85.8580767808588,-4.52973879828343,333.079128052298));
#34509=CARTESIAN_POINT('Ctrl Pts',(85.850257984986,-4.58009824184991,333.207827252327));
#34510=CARTESIAN_POINT('Ctrl Pts',(85.8424458860472,-4.63041455168176,333.336416219264));
#34511=CARTESIAN_POINT('Ctrl Pts',(85.8346337871083,-4.67535450466321,333.467235643882));
#34512=CARTESIAN_POINT('Ctrl Pts',(85.8268216881694,-4.71472404815442,333.599799938489));
#34513=CARTESIAN_POINT('Ctrl Pts',(85.8190150539567,-4.75406605182907,333.732271501608));
#34514=CARTESIAN_POINT('Ctrl Pts',(85.8112084197439,-4.78784529872874,333.866485137799));
#34515=CARTESIAN_POINT('Ctrl Pts',(85.8034017855312,-4.81591686631142,334.001937978241));
#34516=CARTESIAN_POINT('Ctrl Pts',(85.7955983371855,-4.84397697796038,334.137335540732));
#34517=CARTESIAN_POINT('Ctrl Pts',(85.7877948888398,-4.86633397110281,334.273970926373));
#34518=CARTESIAN_POINT('Ctrl Pts',(85.7799914404942,-4.88289356463374,334.41132904016));
#34519=CARTESIAN_POINT('Ctrl Pts',(85.7721889091132,-4.89945121228626,334.548671013323));
#34520=CARTESIAN_POINT('Ctrl Pts',(85.7643863777322,-4.91021276809882,334.686735166231));
#34521=CARTESIAN_POINT('Ctrl Pts',(85.7565838463512,-4.91513558701002,334.824999360551));
#34522=CARTESIAN_POINT('Ctrl Pts',(85.7532346470641,-4.91724868348893,334.884348604845));
#34523=CARTESIAN_POINT('Ctrl Pts',(85.7498854477771,-4.91828663521559,334.943734650103));
#34524=CARTESIAN_POINT('Ctrl Pts',(85.74653624849,-4.91824901287755,335.003116059853));
#34525=CARTESIAN_POINT('',(89.2465362484375,-4.9182497994862,334.998595594818));
#34526=CARTESIAN_POINT('Ctrl Pts',(89.2465362484374,-4.9182497994862,334.998595594818));
#34527=CARTESIAN_POINT('Ctrl Pts',(89.2388185931064,-4.91828848637337,335.134077703145));
#34528=CARTESIAN_POINT('Ctrl Pts',(89.2311009377755,-4.91272478676779,335.269786405984));
#34529=CARTESIAN_POINT('Ctrl Pts',(89.2233832824445,-4.90152866167626,335.405215795924));
#34530=CARTESIAN_POINT('Ctrl Pts',(89.2156749347033,-4.89034603925295,335.540481856309));
#34531=CARTESIAN_POINT('Ctrl Pts',(89.2079665869621,-4.87354453575443,335.675468881894));
#34532=CARTESIAN_POINT('Ctrl Pts',(89.2002582392209,-4.8511460915302,335.809669476472));
#34533=CARTESIAN_POINT('Ctrl Pts',(89.1925572764048,-4.82876910596853,335.943741501172));
#34534=CARTESIAN_POINT('Ctrl Pts',(89.1848563135887,-4.80080591281923,336.077028204597));
#34535=CARTESIAN_POINT('Ctrl Pts',(89.1771553507726,-4.76733033678951,336.209026270362));
#34536=CARTESIAN_POINT('Ctrl Pts',(89.1694598573305,-4.73387853576677,336.340930588528));
#34537=CARTESIAN_POINT('Ctrl Pts',(89.1617643638884,-4.6949222399672,336.471547706784));
#34538=CARTESIAN_POINT('Ctrl Pts',(89.1540688704463,-4.65058645635678,336.600383914706));
#34539=CARTESIAN_POINT('Ctrl Pts',(89.1463761327548,-4.60626654935861,336.729173986475));
#34540=CARTESIAN_POINT('Ctrl Pts',(89.1386833950633,-4.55657111265757,336.856184040658));
#34541=CARTESIAN_POINT('Ctrl Pts',(89.1309906573719,-4.50167509206021,336.980935240745));
#34542=CARTESIAN_POINT('Ctrl Pts',(89.1232990991992,-4.44678748860773,337.105667312871));
#34543=CARTESIAN_POINT('Ctrl Pts',(89.1156075410266,-4.38670104687227,337.228140856245));
#34544=CARTESIAN_POINT('Ctrl Pts',(89.1079159828539,-4.32163877281165,337.347897225142));
#34545=CARTESIAN_POINT('Ctrl Pts',(89.100223878242,-4.25657187646522,337.467662102014));
#34546=CARTESIAN_POINT('Ctrl Pts',(89.0925317736301,-4.18652863431924,337.584709071469));
#34547=CARTESIAN_POINT('Ctrl Pts',(89.0848396690182,-4.11177766731381,337.698604727832));
#34548=CARTESIAN_POINT('Ctrl Pts',(89.0771452919303,-4.03700461665441,337.812534032353));
#34549=CARTESIAN_POINT('Ctrl Pts',(89.0694509148424,-3.95752129254295,337.923309840099));
#34550=CARTESIAN_POINT('Ctrl Pts',(89.0617565377545,-3.8736389428185,338.030528733271));
#34551=CARTESIAN_POINT('Ctrl Pts',(89.0540538399741,-3.78966588279575,338.137863572859));
#34552=CARTESIAN_POINT('Ctrl Pts',(89.0463511421937,-3.70128454467609,338.241633505582));
#34553=CARTESIAN_POINT('Ctrl Pts',(89.0386484444133,-3.60884591006726,338.341468877588));
#34554=CARTESIAN_POINT('Ctrl Pts',(89.0309410313895,-3.51635068870453,338.441365364296));
#34555=CARTESIAN_POINT('Ctrl Pts',(89.0232336183656,-3.41979350602721,338.537322214772));
#34556=CARTESIAN_POINT('Ctrl Pts',(89.0155262053418,-3.31956044271628,338.629008339706));
#34557=CARTESIAN_POINT('Ctrl Pts',(89.0078075361868,-3.21918099611152,338.720828365735));
#34558=CARTESIAN_POINT('Ctrl Pts',(89.0000888670318,-3.11511525407646,338.808364959282));
#34559=CARTESIAN_POINT('Ctrl Pts',(88.9923701978768,-3.00778077722667,338.891328546736));
#34560=CARTESIAN_POINT('Ctrl Pts',(88.988688508236,-2.95658383853328,338.930900936013));
#34561=CARTESIAN_POINT('Ctrl Pts',(88.9850068185952,-2.90464361958345,338.96943354904));
#34562=CARTESIAN_POINT('Ctrl Pts',(88.9813251289544,-2.85200747217322,339.0068986063));
#34563=CARTESIAN_POINT('Ctrl Pts',(88.9735500501759,-2.74084921804736,339.086018195416));
#34564=CARTESIAN_POINT('Ctrl Pts',(88.9657749713975,-2.62622044772756,339.160633722342));
#34565=CARTESIAN_POINT('Ctrl Pts',(88.957999892619,-2.50852224034851,339.230425419763));
#34566=CARTESIAN_POINT('Ctrl Pts',(88.95023438157,-2.39096886810684,339.300131234057));
#34567=CARTESIAN_POINT('Ctrl Pts',(88.942468870521,-2.27035390722286,339.365024832387));
#34568=CARTESIAN_POINT('Ctrl Pts',(88.934703359472,-2.14710959118182,339.424828071909));
#34569=CARTESIAN_POINT('Ctrl Pts',(88.9269455479498,-2.0239874722392,339.484572016345));
#34570=CARTESIAN_POINT('Ctrl Pts',(88.9191877364277,-1.89824153563803,339.53923547646));
#34571=CARTESIAN_POINT('Ctrl Pts',(88.9114299249055,-1.77033063597685,339.588585021749));
#34572=CARTESIAN_POINT('Ctrl Pts',(88.9036779513825,-1.64251599332369,339.637897429941));
#34573=CARTESIAN_POINT('Ctrl Pts',(88.8959259778595,-1.51253999366618,339.681903742773));
#34574=CARTESIAN_POINT('Ctrl Pts',(88.8881740043365,-1.38088327351996,339.720417825512));
#34575=CARTESIAN_POINT('Ctrl Pts',(88.8804253137788,-1.24928231007279,339.758915597515));
#34576=CARTESIAN_POINT('Ctrl Pts',(88.8726766232212,-1.11600241620032,339.791925656085));
#34577=CARTESIAN_POINT('Ctrl Pts',(88.8649279326636,-0.981541056781967,
339.819311176543));
#34578=CARTESIAN_POINT('Ctrl Pts',(88.8571808542858,-0.847107673172575,
339.846690999215));
#34579=CARTESIAN_POINT('Ctrl Pts',(88.8494337759079,-0.711493695729016,
339.868448533491));
#34580=CARTESIAN_POINT('Ctrl Pts',(88.8416866975301,-0.575208109283756,
339.884497793378));
#34581=CARTESIAN_POINT('Ctrl Pts',(88.8339395542243,-0.438921380633828,
339.900547187773));
#34582=CARTESIAN_POINT('Ctrl Pts',(88.8261924109185,-0.301963419947128,
339.910888166642));
#34583=CARTESIAN_POINT('Ctrl Pts',(88.8184452676127,-0.164849289197789,
339.915486524684));
#34584=CARTESIAN_POINT('Ctrl Pts',(88.8106963825846,-0.0277043322809359,
339.920085916535));
#34585=CARTESIAN_POINT('Ctrl Pts',(88.8029474975564,0.109596473985898,339.918940105389));
#34586=CARTESIAN_POINT('Ctrl Pts',(88.7951986125283,0.246537503609198,339.912067011128));
#34587=CARTESIAN_POINT('Ctrl Pts',(88.7874415027536,0.383623883856112,339.905186621694));
#34588=CARTESIAN_POINT('Ctrl Pts',(88.7796843929789,0.520349333637551,339.8925668254));
#34589=CARTESIAN_POINT('Ctrl Pts',(88.7719272832042,0.656202232561501,339.874277555954));
#34590=CARTESIAN_POINT('Ctrl Pts',(88.764166028278,0.792127726930809,339.855978513308));
#34591=CARTESIAN_POINT('Ctrl Pts',(88.7564047733518,0.927179356709075,339.832004029074));
#34592=CARTESIAN_POINT('Ctrl Pts',(88.7486435184257,1.06085612338519,339.802475127263));
#34593=CARTESIAN_POINT('Ctrl Pts',(88.740869848021,1.19474672932282,339.772898988832));
#34594=CARTESIAN_POINT('Ctrl Pts',(88.7330961776164,1.3272576992316,339.737750777714));
#34595=CARTESIAN_POINT('Ctrl Pts',(88.7253225072117,1.45790275785958,339.697201572333));
#34596=CARTESIAN_POINT('Ctrl Pts',(88.7179107030346,1.58246625757705,339.658539942217));
#34597=CARTESIAN_POINT('Ctrl Pts',(88.7104988988575,1.70533338173005,339.61496893066));
#34598=CARTESIAN_POINT('Ctrl Pts',(88.7030870946805,1.82610163012309,339.566676679924));
#34599=CARTESIAN_POINT('Ctrl Pts',(88.695312015902,1.95278909012011,339.516017482124));
#34600=CARTESIAN_POINT('Ctrl Pts',(88.6875369371236,2.07756708358183,339.460002446722));
#34601=CARTESIAN_POINT('Ctrl Pts',(88.6797618583451,2.19994966441851,339.398795805277));
#34602=CARTESIAN_POINT('Ctrl Pts',(88.6719963472961,2.32218164569796,339.337664482502));
#34603=CARTESIAN_POINT('Ctrl Pts',(88.6642308362471,2.44202373319648,339.271354438337));
#34604=CARTESIAN_POINT('Ctrl Pts',(88.6564653251981,2.55900812432425,339.20007862809));
#34605=CARTESIAN_POINT('Ctrl Pts',(88.6487075136759,2.67587652508809,339.128873488017));
#34606=CARTESIAN_POINT('Ctrl Pts',(88.6409497021537,2.78989253648785,339.052712582114));
#34607=CARTESIAN_POINT('Ctrl Pts',(88.6331918906315,2.90061154928129,338.971855448361));
#34608=CARTESIAN_POINT('Ctrl Pts',(88.6254399171085,3.01124724250583,338.891059162166));
#34609=CARTESIAN_POINT('Ctrl Pts',(88.6176879435855,3.11859056123512,338.805573912093));
#34610=CARTESIAN_POINT('Ctrl Pts',(88.6099359700625,3.22222488080447,338.715703147457));
#34611=CARTESIAN_POINT('Ctrl Pts',(88.6021872795049,3.32581531117823,338.625870443144));
#34612=CARTESIAN_POINT('Ctrl Pts',(88.5944385889473,3.42569957184146,338.531656173793));
#34613=CARTESIAN_POINT('Ctrl Pts',(88.5866898983897,3.52149339721162,338.433404624552));
#34614=CARTESIAN_POINT('Ctrl Pts',(88.5789428200118,3.61726729187633,338.335173517366));
#34615=CARTESIAN_POINT('Ctrl Pts',(88.571195741634,3.7089521713491,338.23290708078));
#34616=CARTESIAN_POINT('Ctrl Pts',(88.5634486632562,3.79620028727457,338.126986799044));
#34617=CARTESIAN_POINT('Ctrl Pts',(88.5557015199504,3.88344913442316,338.021065629594));
#34618=CARTESIAN_POINT('Ctrl Pts',(88.5479543766446,3.96626089534252,337.911490855614));
#34619=CARTESIAN_POINT('Ctrl Pts',(88.5402072333388,4.04432807647745,337.798677093256));
#34620=CARTESIAN_POINT('Ctrl Pts',(88.5324583483107,4.12241280877223,337.685837967969));
#34621=CARTESIAN_POINT('Ctrl Pts',(88.5247094632826,4.19575061632469,337.569758726638));
#34622=CARTESIAN_POINT('Ctrl Pts',(88.5169605782545,4.26407753353314,337.450882667636));
#34623=CARTESIAN_POINT('Ctrl Pts',(88.5092034684797,4.33247697363751,337.331880432357));
#34624=CARTESIAN_POINT('Ctrl Pts',(88.501446358705,4.39585470388412,337.210075788828));
#34625=CARTESIAN_POINT('Ctrl Pts',(88.4936892489303,4.45399266586829,337.085936814693));
#34626=CARTESIAN_POINT('Ctrl Pts',(88.4859279940041,4.51216169492042,336.96173150466));
#34627=CARTESIAN_POINT('Ctrl Pts',(88.4781667390779,4.5650852257885,336.835189738904));
#34628=CARTESIAN_POINT('Ctrl Pts',(88.4704054841518,4.61259391110388,336.706798310799));
#34629=CARTESIAN_POINT('Ctrl Pts',(88.4626318137471,4.66017859483271,336.578201498252));
#34630=CARTESIAN_POINT('Ctrl Pts',(88.4548581433424,4.70233100354491,336.447749482818));
#34631=CARTESIAN_POINT('Ctrl Pts',(88.4470844729378,4.73893184929582,336.315943764083));
#34632=CARTESIAN_POINT('Ctrl Pts',(88.4396726687607,4.77382891687134,336.190273633266));
#34633=CARTESIAN_POINT('Ctrl Pts',(88.4322608645836,4.80367957469933,336.063373272853));
#34634=CARTESIAN_POINT('Ctrl Pts',(88.4248490604065,4.82842421967145,335.935682968419));
#34635=CARTESIAN_POINT('Ctrl Pts',(88.4170739816281,4.85438167340417,335.801734181796));
#34636=CARTESIAN_POINT('Ctrl Pts',(88.4092989028497,4.87480196712811,335.666492755274));
#34637=CARTESIAN_POINT('Ctrl Pts',(88.4015238240712,4.88956023335252,335.530456206409));
#34638=CARTESIAN_POINT('Ctrl Pts',(88.3937583130222,4.90430033859078,335.394587059177));
#34639=CARTESIAN_POINT('Ctrl Pts',(88.3859928019732,4.91339223787285,335.257925121314));
#34640=CARTESIAN_POINT('Ctrl Pts',(88.3782272909242,4.91676185503624,335.120979020332));
#34641=CARTESIAN_POINT('Ctrl Pts',(88.370469479402,4.9201281312144,334.984168701809));
#34642=CARTESIAN_POINT('Ctrl Pts',(88.3627116678799,4.91778340662411,334.847075169103));
#34643=CARTESIAN_POINT('Ctrl Pts',(88.3549538563577,4.90970532871861,334.710212754504));
#34644=CARTESIAN_POINT('Ctrl Pts',(88.3472018828347,4.90163332982287,334.573453333212));
#34645=CARTESIAN_POINT('Ctrl Pts',(88.3394499093116,4.88783658841117,334.436925072465));
#34646=CARTESIAN_POINT('Ctrl Pts',(88.3316979357886,4.86834482197517,334.30114253467));
#34647=CARTESIAN_POINT('Ctrl Pts',(88.323949245231,4.84886131031385,334.16541750086));
#34648=CARTESIAN_POINT('Ctrl Pts',(88.3162005546733,4.82368762604653,334.030437947972));
#34649=CARTESIAN_POINT('Ctrl Pts',(88.3084518641157,4.79290533774092,333.896713325579));
#34650=CARTESIAN_POINT('Ctrl Pts',(88.3007047857379,4.76212945394752,333.763016525711));
#34651=CARTESIAN_POINT('Ctrl Pts',(88.2929577073601,4.72574737482395,333.630574517668));
#34652=CARTESIAN_POINT('Ctrl Pts',(88.2852106289822,4.68389171202491,333.499886173477));
#34653=CARTESIAN_POINT('Ctrl Pts',(88.2774634856764,4.64203569843513,333.369196733993));
#34654=CARTESIAN_POINT('Ctrl Pts',(88.2697163423706,4.59470612889139,333.240261359924));
#34655=CARTESIAN_POINT('Ctrl Pts',(88.2619691990648,4.54208526055444,333.113563001753));
#34656=CARTESIAN_POINT('Ctrl Pts',(88.2542203140368,4.48945256192923,332.986836159102));
#34657=CARTESIAN_POINT('Ctrl Pts',(88.2464714290087,4.43152634724096,332.862347694028));
#34658=CARTESIAN_POINT('Ctrl Pts',(88.2387225439806,4.36853654861631,332.740559475024));
#34659=CARTESIAN_POINT('Ctrl Pts',(88.2309654342059,4.30547989196838,332.618641988746));
#34660=CARTESIAN_POINT('Ctrl Pts',(88.2232083244311,4.23734909508655,332.499430821514));
#34661=CARTESIAN_POINT('Ctrl Pts',(88.2154512146564,4.16441977053293,332.383362646966));
#34662=CARTESIAN_POINT('Ctrl Pts',(88.2076899597302,4.09145147488014,332.267232449296));
#34663=CARTESIAN_POINT('Ctrl Pts',(88.199928704804,4.01367976371038,332.154248912699));
#34664=CARTESIAN_POINT('Ctrl Pts',(88.1921674498779,3.93142234837809,332.044817876818));
#34665=CARTESIAN_POINT('Ctrl Pts',(88.1843937794732,3.84903334798889,331.935211786943));
#34666=CARTESIAN_POINT('Ctrl Pts',(88.1766201090686,3.76214455219782,331.829169856289));
#34667=CARTESIAN_POINT('Ctrl Pts',(88.1688464386639,3.67111312915359,331.727063786834));
#34668=CARTESIAN_POINT('Ctrl Pts',(88.1614346344868,3.58431924075284,331.629710779477));
#34669=CARTESIAN_POINT('Ctrl Pts',(88.1540228303097,3.49375992416188,331.535935657913));
#34670=CARTESIAN_POINT('Ctrl Pts',(88.1466110261326,3.39977317025234,331.446026807454));
#34671=CARTESIAN_POINT('Ctrl Pts',(88.1388359473541,3.30117984556167,331.351711256411));
#34672=CARTESIAN_POINT('Ctrl Pts',(88.1310608685757,3.19850303740045,331.261352499728));
#34673=CARTESIAN_POINT('Ctrl Pts',(88.1232857897973,3.0920935459301,331.17532477644));
#34674=CARTESIAN_POINT('Ctrl Pts',(88.1155202787482,2.98581499811352,331.089402915741));
#34675=CARTESIAN_POINT('Ctrl Pts',(88.1077547676992,2.87581320740411,331.00780172743));
#34676=CARTESIAN_POINT('Ctrl Pts',(88.0999892566502,2.76247580266768,330.930858751263));
#34677=CARTESIAN_POINT('Ctrl Pts',(88.092231445128,2.64925077229818,330.853992064281));
#34678=CARTESIAN_POINT('Ctrl Pts',(88.0844736336059,2.53269703086678,330.781774616238));
#34679=CARTESIAN_POINT('Ctrl Pts',(88.0767158220837,2.41323499512445,330.714503538584));
#34680=CARTESIAN_POINT('Ctrl Pts',(88.0689638485607,2.29386285835253,330.647283084549));
#34681=CARTESIAN_POINT('Ctrl Pts',(88.0612118750377,2.17158712275385,330.585001782863));
#34682=CARTESIAN_POINT('Ctrl Pts',(88.0534599015147,2.04685657667291,330.527913102697));
#34683=CARTESIAN_POINT('Ctrl Pts',(88.0457112109571,1.92217885405213,330.47084859962));
#34684=CARTESIAN_POINT('Ctrl Pts',(88.0379625203995,1.7950487433436,330.418972506585));
#34685=CARTESIAN_POINT('Ctrl Pts',(88.0302138298419,1.66593879299465,330.372491923238));
#34686=CARTESIAN_POINT('Ctrl Pts',(88.022466751464,1.53685570504896,330.326021010565));
#34687=CARTESIAN_POINT('Ctrl Pts',(88.0147196730862,1.40579396434206,330.284943507005));
#34688=CARTESIAN_POINT('Ctrl Pts',(88.0069725947084,1.27324484678053,330.249417864867));
#34689=CARTESIAN_POINT('Ctrl Pts',(87.9992254514026,1.14069461832972,330.21389192499));
#34690=CARTESIAN_POINT('Ctrl Pts',(87.9914783080968,1.00665736570963,330.183918040532));
#34691=CARTESIAN_POINT('Ctrl Pts',(87.983731164791,0.87163784209063,330.159604299777));
#34692=CARTESIAN_POINT('Ctrl Pts',(87.9759822797629,0.736587963216725,330.135285092777));
#34693=CARTESIAN_POINT('Ctrl Pts',(87.9682333947348,0.600555758517896,330.116628630912));
#34694=CARTESIAN_POINT('Ctrl Pts',(87.9604845097067,0.464054052530329,330.103691502894));
#34695=CARTESIAN_POINT('Ctrl Pts',(87.952727399932,0.327407462221328,330.090740643275));
#34696=CARTESIAN_POINT('Ctrl Pts',(87.9449702901573,0.190290764900753,330.083521280956));
#34697=CARTESIAN_POINT('Ctrl Pts',(87.9372131803826,0.0532203185172771,
330.082037956613));
#34698=CARTESIAN_POINT('Ctrl Pts',(87.9294519254564,-0.0839233739299897,
330.080553839629));
#34699=CARTESIAN_POINT('Ctrl Pts',(87.9216906705302,-0.221020375705536,
330.084811856092));
#34700=CARTESIAN_POINT('Ctrl Pts',(87.9139294156041,-0.357557475752364,
330.094764458863));
#34701=CARTESIAN_POINT('Ctrl Pts',(87.9061557451994,-0.494312990662116,
330.104732982555));
#34702=CARTESIAN_POINT('Ctrl Pts',(87.8983820747948,-0.630506425535559,
330.120414251265));
#34703=CARTESIAN_POINT('Ctrl Pts',(87.8906084043901,-0.765631924068881,
330.141709063946));
#34704=CARTESIAN_POINT('Ctrl Pts',(87.8831966002129,-0.894467298137263,
330.162012597973));
#34705=CARTESIAN_POINT('Ctrl Pts',(87.8757847960358,-1.02233164096596,330.187418760199));
#34706=CARTESIAN_POINT('Ctrl Pts',(87.8683729918586,-1.14879953693754,330.21779938873));
#34707=CARTESIAN_POINT('Ctrl Pts',(87.8605979130802,-1.2814660012179,330.249669062364));
#34708=CARTESIAN_POINT('Ctrl Pts',(87.8528228343018,-1.41301491992177,330.287113872835));
#34709=CARTESIAN_POINT('Ctrl Pts',(87.8450477555233,-1.54294174936587,330.330041347018));
#34710=CARTESIAN_POINT('Ctrl Pts',(87.8372822444743,-1.6727086955747,330.372915996211));
#34711=CARTESIAN_POINT('Ctrl Pts',(87.8295167334254,-1.80085715656524,330.421259763533));
#34712=CARTESIAN_POINT('Ctrl Pts',(87.8217512223764,-1.92689351973213,330.474929345732));
#34713=CARTESIAN_POINT('Ctrl Pts',(87.8139934108542,-2.052804917478,330.528545714385));
#34714=CARTESIAN_POINT('Ctrl Pts',(87.806235599332,-2.17660802756939,330.587477237147));
#34715=CARTESIAN_POINT('Ctrl Pts',(87.7984777878098,-2.29782547420462,330.651531171482));
#34716=CARTESIAN_POINT('Ctrl Pts',(87.7907258142868,-2.41895170086708,330.715536903199));
#34717=CARTESIAN_POINT('Ctrl Pts',(87.7829738407638,-2.53749579288089,330.78465719186));
#34718=CARTESIAN_POINT('Ctrl Pts',(87.7752218672408,-2.65300173748832,330.858651808483));
#34719=CARTESIAN_POINT('Ctrl Pts',(87.7674731766832,-2.76845876525978,330.932615088342));
#34720=CARTESIAN_POINT('Ctrl Pts',(87.7597244861256,-2.88087987624982,331.011448380047));
#34721=CARTESIAN_POINT('Ctrl Pts',(87.751975795568,-2.98983519286681,331.094866381032));
#34722=CARTESIAN_POINT('Ctrl Pts',(87.7442287171902,-3.09876784042016,331.178267026204));
#34723=CARTESIAN_POINT('Ctrl Pts',(87.7364816388123,-3.20423581773168,331.266250245841));
#34724=CARTESIAN_POINT('Ctrl Pts',(87.7287345604345,-3.30584002129114,331.358488663188));
#34725=CARTESIAN_POINT('Ctrl Pts',(87.7209874171287,-3.40744507639217,331.450727853582));
#34726=CARTESIAN_POINT('Ctrl Pts',(87.7132402738228,-3.50518600374606,331.547222050089));
#34727=CARTESIAN_POINT('Ctrl Pts',(87.705493130517,-3.59869875870711,331.647605287771));
#34728=CARTESIAN_POINT('Ctrl Pts',(87.6977442454889,-3.69223253732062,331.748011093736));
#34729=CARTESIAN_POINT('Ctrl Pts',(87.6899953604608,-3.78153598561045,331.852307394765));
#34730=CARTESIAN_POINT('Ctrl Pts',(87.6822464754326,-3.8662839981385,331.960093569164));
#34731=CARTESIAN_POINT('Ctrl Pts',(87.6744893656579,-3.95112196308247,332.067994148922));
#34732=CARTESIAN_POINT('Ctrl Pts',(87.6667322558832,-4.03139459154995,332.179391693757));
#34733=CARTESIAN_POINT('Ctrl Pts',(87.6589751461085,-4.10681863427376,332.293854444476));
#34734=CARTESIAN_POINT('Ctrl Pts',(87.6512138911824,-4.18228298119431,332.408378360429));
#34735=CARTESIAN_POINT('Ctrl Pts',(87.6434526362562,-4.25289337859473,332.525970411091));
#34736=CARTESIAN_POINT('Ctrl Pts',(87.63569138133,-4.31841208192752,332.646173295852));
#34737=CARTESIAN_POINT('Ctrl Pts',(87.6279177109253,-4.38403559383318,332.766568466054));
#34738=CARTESIAN_POINT('Ctrl Pts',(87.6201440405207,-4.44455096281739,332.889582465288));
#34739=CARTESIAN_POINT('Ctrl Pts',(87.612370370116,-4.49976786128482,333.014736224818));
#34740=CARTESIAN_POINT('Ctrl Pts',(87.6049585659389,-4.55241439984428,333.134064046733));
#34741=CARTESIAN_POINT('Ctrl Pts',(87.5975467617618,-4.60024454877045,333.255336632668));
#34742=CARTESIAN_POINT('Ctrl Pts',(87.5901349575847,-4.64313586533308,333.378126885802));
#34743=CARTESIAN_POINT('Ctrl Pts',(87.5810267921634,-4.69584384264283,333.529020502383));
#34744=CARTESIAN_POINT('Ctrl Pts',(87.5719186267421,-4.74123094441884,333.682596029949));
#34745=CARTESIAN_POINT('Ctrl Pts',(87.5628104613208,-4.77905702408711,333.838192346804));
#34746=CARTESIAN_POINT('Ctrl Pts',(87.5537431289365,-4.81671352474134,333.993091106043));
#34747=CARTESIAN_POINT('Ctrl Pts',(87.5446757965522,-4.84687655935502,334.14999248358));
#34748=CARTESIAN_POINT('Ctrl Pts',(87.5356084641679,-4.86935592408862,334.308222617424));
#34749=CARTESIAN_POINT('Ctrl Pts',(87.5266169340333,-4.8916473629422,334.465129958676));
#34750=CARTESIAN_POINT('Ctrl Pts',(87.5176254038986,-4.90638298903107,334.623343823302));
#34751=CARTESIAN_POINT('Ctrl Pts',(87.508633873764,-4.91342453997809,334.782187345544));
#34752=CARTESIAN_POINT('Ctrl Pts',(87.5046013320235,-4.91658255064887,334.853425847118));
#34753=CARTESIAN_POINT('Ctrl Pts',(87.5005687902829,-4.91819364564975,334.924790739551));
#34754=CARTESIAN_POINT('Ctrl Pts',(87.4965362485424,-4.91824854721736,334.996219749433));
#34755=CARTESIAN_POINT('',(90.9965362484616,-4.91824791233306,335.004531592596));
#34756=CARTESIAN_POINT('Ctrl Pts',(90.9965362484616,-4.91824791233306,335.004531592596));
#34757=CARTESIAN_POINT('Ctrl Pts',(90.9864706741919,-4.91808413604804,335.182281987159));
#34758=CARTESIAN_POINT('Ctrl Pts',(90.9764050999222,-4.90828083222216,335.359603187475));
#34759=CARTESIAN_POINT('Ctrl Pts',(90.9663395256525,-4.88899777647855,335.53561535087));
#34760=CARTESIAN_POINT('Ctrl Pts',(90.956026782763,-4.86924120912543,335.715949640586));
#34761=CARTESIAN_POINT('Ctrl Pts',(90.9457140398736,-4.83953357743045,335.894910145243));
#34762=CARTESIAN_POINT('Ctrl Pts',(90.9354012969841,-4.80009451970844,336.07157625224));
#34763=CARTESIAN_POINT('Ctrl Pts',(90.9332646542801,-4.7919233497454,336.108178769399));
#34764=CARTESIAN_POINT('Ctrl Pts',(90.9311280115761,-4.78333461513977,336.144682874129));
#34765=CARTESIAN_POINT('Ctrl Pts',(90.9289913688721,-4.77433052225825,336.181080491217));
#34766=CARTESIAN_POINT('Ctrl Pts',(90.9212162900936,-4.7415653194704,336.313528625702));
#34767=CARTESIAN_POINT('Ctrl Pts',(90.9134412113152,-4.70323265688646,336.444821576094));
#34768=CARTESIAN_POINT('Ctrl Pts',(90.9056661325368,-4.65942841407308,336.574455434945));
#34769=CARTESIAN_POINT('Ctrl Pts',(90.8979006214878,-4.61567807516919,336.70392977108));
#34770=CARTESIAN_POINT('Ctrl Pts',(90.8901351104388,-4.56646967696209,336.831748711144));
#34771=CARTESIAN_POINT('Ctrl Pts',(90.8823695993897,-4.51194985413787,336.957419621912));
#34772=CARTESIAN_POINT('Ctrl Pts',(90.8746117878675,-4.45748408787668,337.082965929605));
#34773=CARTESIAN_POINT('Ctrl Pts',(90.8668539763453,-4.39771753178151,337.206368090105));
#34774=CARTESIAN_POINT('Ctrl Pts',(90.8590961648231,-4.33284614900619,337.327150040617));
#34775=CARTESIAN_POINT('Ctrl Pts',(90.8513441913001,-4.26802358400369,337.44784109888));
#34776=CARTESIAN_POINT('Ctrl Pts',(90.8435922177771,-4.19810402293034,337.565915528946));
#34777=CARTESIAN_POINT('Ctrl Pts',(90.8358402442541,-4.12333076997611,337.68091895138));
#34778=CARTESIAN_POINT('Ctrl Pts',(90.8280915536965,-4.04858918353885,337.795873669797));
#34779=CARTESIAN_POINT('Ctrl Pts',(90.8203428631388,-3.96899820616832,337.907759640314));
#34780=CARTESIAN_POINT('Ctrl Pts',(90.8125941725812,-3.88484603805112,338.016148922573));
#34781=CARTESIAN_POINT('Ctrl Pts',(90.8048470942034,-3.80071137849535,338.124515653536));
#34782=CARTESIAN_POINT('Ctrl Pts',(90.7971000158255,-3.71201765536447,338.229386834769));
#34783=CARTESIAN_POINT('Ctrl Pts',(90.7893529374477,-3.61909493417,338.330365583531));
#34784=CARTESIAN_POINT('Ctrl Pts',(90.7816057941419,-3.5261714341937,338.431345178591));
#34785=CARTESIAN_POINT('Ctrl Pts',(90.7738586508361,-3.42901913013828,338.528431988489));
#34786=CARTESIAN_POINT('Ctrl Pts',(90.7661115075303,-3.32800643797098,338.621264449239));
#34787=CARTESIAN_POINT('Ctrl Pts',(90.7583626225022,-3.22697103600585,338.714117780697));
#34788=CARTESIAN_POINT('Ctrl Pts',(90.750613737474,-3.12207380665144,338.802714595304));
#34789=CARTESIAN_POINT('Ctrl Pts',(90.7428648524459,-3.01371755877787,338.886732501525));
#34790=CARTESIAN_POINT('Ctrl Pts',(90.7351077426712,-2.90524630046335,338.97083958522));
#34791=CARTESIAN_POINT('Ctrl Pts',(90.7273506328964,-2.79330899897093,339.050357812131));
#34792=CARTESIAN_POINT('Ctrl Pts',(90.7195935231217,-2.67833931719225,339.125006856295));
#34793=CARTESIAN_POINT('Ctrl Pts',(90.7118322681955,-2.56330819929157,339.199695790522));
#34794=CARTESIAN_POINT('Ctrl Pts',(90.7040710132694,-2.4452418085812,339.269510158561));
#34795=CARTESIAN_POINT('Ctrl Pts',(90.6963097583432,-2.32459904137099,339.334215310683));
#34796=CARTESIAN_POINT('Ctrl Pts',(90.6885360879385,-2.20376328505072,339.39902396996));
#34797=CARTESIAN_POINT('Ctrl Pts',(90.6807624175338,-2.08034326860222,339.45870691083));
#34798=CARTESIAN_POINT('Ctrl Pts',(90.6729887471292,-1.95481933562801,339.51307704649));
#34799=CARTESIAN_POINT('Ctrl Pts',(90.6655769429521,-1.83513857193331,339.564916239254));
#34800=CARTESIAN_POINT('Ctrl Pts',(90.658165138775,-1.7135456267381,339.61192601403));
#34801=CARTESIAN_POINT('Ctrl Pts',(90.6507533345979,-1.590468414307,339.653986816225));
#34802=CARTESIAN_POINT('Ctrl Pts',(90.6429782558195,-1.46135882106628,339.698109143627));
#34803=CARTESIAN_POINT('Ctrl Pts',(90.6352031770411,-1.33020777481749,339.736924538914));
#34804=CARTESIAN_POINT('Ctrl Pts',(90.6274280982626,-1.19749090801891,339.770240936023));
#34805=CARTESIAN_POINT('Ctrl Pts',(90.6196625872136,-1.06493735777411,339.803516335185));
#34806=CARTESIAN_POINT('Ctrl Pts',(90.6118970761646,-0.93082219632958,339.831306106035));
#34807=CARTESIAN_POINT('Ctrl Pts',(90.6041315651156,-0.795639041917121,
339.853466964704));
#34808=CARTESIAN_POINT('Ctrl Pts',(90.5963737535934,-0.660589921995745,
339.875605850818));
#34809=CARTESIAN_POINT('Ctrl Pts',(90.5886159420712,-0.524475299654361,
339.892126868595));
#34810=CARTESIAN_POINT('Ctrl Pts',(90.580858130549,-0.387801553160386,339.902937182737));
#34811=CARTESIAN_POINT('Ctrl Pts',(90.573106157026,-0.2512306579951,339.913739361775));
#34812=CARTESIAN_POINT('Ctrl Pts',(90.565354183503,-0.114101864265123,339.918839360418));
#34813=CARTESIAN_POINT('Ctrl Pts',(90.55760220998,0.0230710648120109,339.918195887566));
#34814=CARTESIAN_POINT('Ctrl Pts',(90.5498535194224,0.160185901072334,339.917552687224));
#34815=CARTESIAN_POINT('Ctrl Pts',(90.5421048288647,0.297344445447526,339.911170855017));
#34816=CARTESIAN_POINT('Ctrl Pts',(90.5343561383071,0.434030872101439,339.899061161545));
#34817=CARTESIAN_POINT('Ctrl Pts',(90.5266090599293,0.570688860002659,339.886953987597));
#34818=CARTESIAN_POINT('Ctrl Pts',(90.5188619815514,0.706874536460283,339.86912135729));
#34819=CARTESIAN_POINT('Ctrl Pts',(90.5111149031736,0.842075536924039,339.845626053733));
#34820=CARTESIAN_POINT('Ctrl Pts',(90.5033677598678,0.977277670502308,339.822130553262));
#34821=CARTESIAN_POINT('Ctrl Pts',(90.495620616562,1.11149472652386,339.792972351804));
#34822=CARTESIAN_POINT('Ctrl Pts',(90.4878734732562,1.24422328710095,339.758265595187));
#34823=CARTESIAN_POINT('Ctrl Pts',(90.4801245882281,1.37698168787638,339.723551035753));
#34824=CARTESIAN_POINT('Ctrl Pts',(90.4723757032,1.50825054921469,339.683285537773));
#34825=CARTESIAN_POINT('Ctrl Pts',(90.4646268181719,1.63754078220388,339.63763336726));
#34826=CARTESIAN_POINT('Ctrl Pts',(90.4568697083972,1.76696824518228,339.591932741061));
#34827=CARTESIAN_POINT('Ctrl Pts',(90.4491125986225,1.89441251543709,339.540834151494));
#34828=CARTESIAN_POINT('Ctrl Pts',(90.4413554888477,2.01940318101161,339.484550574475));
#34829=CARTESIAN_POINT('Ctrl Pts',(90.4335942339216,2.1444606376013,339.428236921311));
#34830=CARTESIAN_POINT('Ctrl Pts',(90.4258329789954,2.26706152777124,339.36673293502));
#34831=CARTESIAN_POINT('Ctrl Pts',(90.4180717240692,2.38676019443191,339.300297528867));
#34832=CARTESIAN_POINT('Ctrl Pts',(90.4102980536645,2.50665033994954,339.233755847714));
#34833=CARTESIAN_POINT('Ctrl Pts',(90.4025243832599,2.62362865094576,339.162267186743));
#34834=CARTESIAN_POINT('Ctrl Pts',(90.3947507128552,2.73727786065232,339.086134233733));
#34835=CARTESIAN_POINT('Ctrl Pts',(90.3873389086782,2.84563667230385,339.013545288002));
#34836=CARTESIAN_POINT('Ctrl Pts',(90.3799271045011,2.95096911446867,338.936734872868));
#34837=CARTESIAN_POINT('Ctrl Pts',(90.3725153003241,3.05294308217669,338.855998132713));
#34838=CARTESIAN_POINT('Ctrl Pts',(90.3647402215457,3.15991509780755,338.771304244421));
#34839=CARTESIAN_POINT('Ctrl Pts',(90.3569651427673,3.26352914836477,338.682021769262));
#34840=CARTESIAN_POINT('Ctrl Pts',(90.3491900639888,3.36336632938506,338.588446738752));
#34841=CARTESIAN_POINT('Ctrl Pts',(90.3414245529398,3.46308065439822,338.494986858274));
#34842=CARTESIAN_POINT('Ctrl Pts',(90.3336590418908,3.55902707495898,338.397245197377));
#34843=CARTESIAN_POINT('Ctrl Pts',(90.3258935308418,3.65081797545538,338.295559311041));
#34844=CARTESIAN_POINT('Ctrl Pts',(90.3181357193196,3.74251786500662,338.193974246558));
#34845=CARTESIAN_POINT('Ctrl Pts',(90.3103779077974,3.83007017371988,338.088453027448));
#34846=CARTESIAN_POINT('Ctrl Pts',(90.3026200962752,3.91312280407602,337.979371239493));
#34847=CARTESIAN_POINT('Ctrl Pts',(90.2948681227522,3.996112934694,337.870371539043));
#34848=CARTESIAN_POINT('Ctrl Pts',(90.2871161492292,4.07460989109229,337.757816912785));
#34849=CARTESIAN_POINT('Ctrl Pts',(90.2793641757062,4.14830092394737,337.642117050185));
#34850=CARTESIAN_POINT('Ctrl Pts',(90.2716154851486,4.22196074860629,337.526466186545));
#34851=CARTESIAN_POINT('Ctrl Pts',(90.2638667945909,4.29081848826982,337.407673064834));
#34852=CARTESIAN_POINT('Ctrl Pts',(90.2561181040333,4.35460405720851,337.286177282593));
#34853=CARTESIAN_POINT('Ctrl Pts',(90.2483710256555,4.41837635502684,337.164706778563));
#34854=CARTESIAN_POINT('Ctrl Pts',(90.2406239472776,4.47707839962336,337.040535078341));
#34855=CARTESIAN_POINT('Ctrl Pts',(90.2328768688998,4.53048571679436,336.91412701575));
#34856=CARTESIAN_POINT('Ctrl Pts',(90.225129725594,4.58389348157008,336.787717893737));
#34857=CARTESIAN_POINT('Ctrl Pts',(90.2173825822882,4.63200627828735,336.659072732027));
#34858=CARTESIAN_POINT('Ctrl Pts',(90.2096354389824,4.67464766630308,336.528676636319));
#34859=CARTESIAN_POINT('Ctrl Pts',(90.2018865539544,4.71729864100816,336.3982512248));
#34860=CARTESIAN_POINT('Ctrl Pts',(90.1941376689262,4.75447563780562,336.266074467412));
#34861=CARTESIAN_POINT('Ctrl Pts',(90.1863887838982,4.78605211741718,336.132646543219));
#34862=CARTESIAN_POINT('Ctrl Pts',(90.1786316741234,4.81766211263045,335.99907699725));
#34863=CARTESIAN_POINT('Ctrl Pts',(90.1708745643487,4.84365962590922,335.864254012637));
#34864=CARTESIAN_POINT('Ctrl Pts',(90.1631174545739,4.86396918634112,335.728688422321));
#34865=CARTESIAN_POINT('Ctrl Pts',(90.1553561996478,4.88428959955274,335.593050390087));
#34866=CARTESIAN_POINT('Ctrl Pts',(90.1475949447216,4.89891596185973,335.456669349888));
#34867=CARTESIAN_POINT('Ctrl Pts',(90.1398336897955,4.90782482832607,335.320060177101));
#34868=CARTESIAN_POINT('Ctrl Pts',(90.1320600193908,4.91674794607535,335.183232474159));
#34869=CARTESIAN_POINT('Ctrl Pts',(90.1242863489861,4.9199352822153,335.04617630035));
#34870=CARTESIAN_POINT('Ctrl Pts',(90.1165126785815,4.9174155663663,334.909406345927));
#34871=CARTESIAN_POINT('Ctrl Pts',(90.1091008744043,4.91501314389626,334.779003065785));
#34872=CARTESIAN_POINT('Ctrl Pts',(90.1016890702272,4.90742305556099,334.648860244988));
#34873=CARTESIAN_POINT('Ctrl Pts',(90.0942772660501,4.89471377351411,334.519416877251));
#34874=CARTESIAN_POINT('Ctrl Pts',(90.0865021872716,4.88138157169519,334.38362910447));
#34875=CARTESIAN_POINT('Ctrl Pts',(90.0787271084932,4.8623735417055,334.248181968511));
#34876=CARTESIAN_POINT('Ctrl Pts',(90.0709520297147,4.83771192951968,334.113587934715));
#34877=CARTESIAN_POINT('Ctrl Pts',(90.0631865186657,4.81308066501769,333.979159527446));
#34878=CARTESIAN_POINT('Ctrl Pts',(90.0554210076167,4.78280973071296,333.845582514343));
#34879=CARTESIAN_POINT('Ctrl Pts',(90.0476554965677,4.74697322273925,333.713365520011));
#34880=CARTESIAN_POINT('Ctrl Pts',(90.0398976850455,4.71117224676752,333.581279619214));
#34881=CARTESIAN_POINT('Ctrl Pts',(90.0321398735233,4.66981678041663,333.450551428504));
#34882=CARTESIAN_POINT('Ctrl Pts',(90.0243820620011,4.62303212161206,333.321680285213));
#34883=CARTESIAN_POINT('Ctrl Pts',(90.0166300884781,4.57628266974691,333.192906121544));
#34884=CARTESIAN_POINT('Ctrl Pts',(90.0088781149551,4.52411229053993,333.065986589598));
#34885=CARTESIAN_POINT('Ctrl Pts',(90.0011261414321,4.46669625399965,332.941406393431));
#34886=CARTESIAN_POINT('Ctrl Pts',(89.9933774508745,4.40930453318493,332.816878957052));
#34887=CARTESIAN_POINT('Ctrl Pts',(89.9856287603168,4.34667173678616,332.694689240247));
#34888=CARTESIAN_POINT('Ctrl Pts',(89.9778800697592,4.27902137286804,332.575302255324));
#34889=CARTESIAN_POINT('Ctrl Pts',(89.9701329913814,4.21138508417316,332.455940109859));
#34890=CARTESIAN_POINT('Ctrl Pts',(89.9623859130035,4.13873349702308,332.339379876244));
#34891=CARTESIAN_POINT('Ctrl Pts',(89.9546388346257,4.06133602422417,332.226061867878));
#34892=CARTESIAN_POINT('Ctrl Pts',(89.9468916913199,3.98393790275988,332.112742909798));
#34893=CARTESIAN_POINT('Ctrl Pts',(89.9391445480141,3.90179403676904,332.002666553938));
#34894=CARTESIAN_POINT('Ctrl Pts',(89.9313974047083,3.81521687982707,331.896243691528));
#34895=CARTESIAN_POINT('Ctrl Pts',(89.9236485196802,3.72862025850221,331.789796902998));
#34896=CARTESIAN_POINT('Ctrl Pts',(89.9158996346521,3.63758860952924,331.687005545531));
#34897=CARTESIAN_POINT('Ctrl Pts',(89.908150749624,3.54247406649159,331.588246704298));
#34898=CARTESIAN_POINT('Ctrl Pts',(89.9003936398493,3.44725856789517,331.48938303941));
#34899=CARTESIAN_POINT('Ctrl Pts',(89.8926365300745,3.34795178998452,331.394560722746));
#34900=CARTESIAN_POINT('Ctrl Pts',(89.8848794202998,3.24494246143393,331.304119660421));
#34901=CARTESIAN_POINT('Ctrl Pts',(89.8771181653736,3.14187808799183,331.213630269285));
#34902=CARTESIAN_POINT('Ctrl Pts',(89.8693569104475,3.03510752563133,331.127527042787));
#34903=CARTESIAN_POINT('Ctrl Pts',(89.8615956555213,2.92505105664167,331.046108324886));
#34904=CARTESIAN_POINT('Ctrl Pts',(89.8538219851167,2.81481853316894,330.96455936357));
#34905=CARTESIAN_POINT('Ctrl Pts',(89.846048314712,2.70128992312181,330.887710104681));
#34906=CARTESIAN_POINT('Ctrl Pts',(89.8382746443073,2.58491358776074,330.815814917298));
#34907=CARTESIAN_POINT('Ctrl Pts',(89.8308628401303,2.47395459881013,330.747266468184));
#34908=CARTESIAN_POINT('Ctrl Pts',(89.8234510359533,2.36040729201062,330.683221387467));
#34909=CARTESIAN_POINT('Ctrl Pts',(89.8160392317762,2.2446778807548,330.62385966014));
#34910=CARTESIAN_POINT('Ctrl Pts',(89.8082641529978,2.12327622631235,330.561588437727));
#34911=CARTESIAN_POINT('Ctrl Pts',(89.8004890742194,1.99908950433923,330.504274478442));
#34912=CARTESIAN_POINT('Ctrl Pts',(89.7927139954409,1.87256069644547,330.45217639957));
#34913=CARTESIAN_POINT('Ctrl Pts',(89.7849484843919,1.74618759030504,330.400142430701));
#34914=CARTESIAN_POINT('Ctrl Pts',(89.7771829733429,1.61747849074813,330.353311718723));
#34915=CARTESIAN_POINT('Ctrl Pts',(89.7694174622939,1.48690120872592,330.311897200574));
#34916=CARTESIAN_POINT('Ctrl Pts',(89.7616596507717,1.35645339445901,330.27052374504));
#34917=CARTESIAN_POINT('Ctrl Pts',(89.7539018392496,1.22414145410857,330.234555913799));
#34918=CARTESIAN_POINT('Ctrl Pts',(89.7461440277274,1.09045309698793,330.204158561236));
#34919=CARTESIAN_POINT('Ctrl Pts',(89.7383920542043,0.956865344595516,330.173784083644));
#34920=CARTESIAN_POINT('Ctrl Pts',(89.7306400806814,0.821903616748002,330.148971827148));
#34921=CARTESIAN_POINT('Ctrl Pts',(89.7228881071583,0.686070360086097,330.129836704636));
#34922=CARTESIAN_POINT('Ctrl Pts',(89.7151394166007,0.550294628889126,330.11070968586));
#34923=CARTESIAN_POINT('Ctrl Pts',(89.7073907260431,0.41364848922479,330.097255073556));
#34924=CARTESIAN_POINT('Ctrl Pts',(89.6996420354855,0.276643932899942,330.089536559866));
#34925=CARTESIAN_POINT('Ctrl Pts',(89.6918949571076,0.139667881517228,330.081819652078));
#34926=CARTESIAN_POINT('Ctrl Pts',(89.6841478787298,0.00233395181259097,
330.079836491032));
#34927=CARTESIAN_POINT('Ctrl Pts',(89.676400800352,-0.134841792553407,330.083598800598));
#34928=CARTESIAN_POINT('Ctrl Pts',(89.6686536570462,-0.272018686584173,
330.087361141696));
#34929=CARTESIAN_POINT('Ctrl Pts',(89.6609065137404,-0.409037001904642,
330.096869038734));
#34930=CARTESIAN_POINT('Ctrl Pts',(89.6531593704346,-0.545382124755205,
330.112082099657));
#34931=CARTESIAN_POINT('Ctrl Pts',(89.6454104854065,-0.681757900883981,
330.127298580798));
#34932=CARTESIAN_POINT('Ctrl Pts',(89.6376616003784,-0.817459794989565,
330.148222734802));
#34933=CARTESIAN_POINT('Ctrl Pts',(89.6299127153503,-0.951980148418879,
330.174762507449));
#34934=CARTESIAN_POINT('Ctrl Pts',(89.6221556055756,-1.08664328314127,330.201330449686));
#34935=CARTESIAN_POINT('Ctrl Pts',(89.6143984958009,-1.22012198791813,330.233525841398));
#34936=CARTESIAN_POINT('Ctrl Pts',(89.6066413860261,-1.35192006505528,330.271205735052));
#34937=CARTESIAN_POINT('Ctrl Pts',(89.5988801311,-1.48378857087077,330.308905763637));
#34938=CARTESIAN_POINT('Ctrl Pts',(89.5911188761738,-1.61397428875126,330.352096010916));
#34939=CARTESIAN_POINT('Ctrl Pts',(89.5833576212476,-1.74199889603575,330.40058450358));
#34940=CARTESIAN_POINT('Ctrl Pts',(89.575583950843,-1.87022830096878,330.449150562029));
#34941=CARTESIAN_POINT('Ctrl Pts',(89.5678102804383,-1.99628932744208,330.50303164865));
#34942=CARTESIAN_POINT('Ctrl Pts',(89.5600366100336,-2.11972543706607,330.561988380597));
#34943=CARTESIAN_POINT('Ctrl Pts',(89.5526248058565,-2.23741556609071,330.618200662488));
#34944=CARTESIAN_POINT('Ctrl Pts',(89.5452130016794,-2.35271940386158,330.67902654712));
#34945=CARTESIAN_POINT('Ctrl Pts',(89.5378011975023,-2.46526577178178,330.744221841193));
#34946=CARTESIAN_POINT('Ctrl Pts',(89.5300261187238,-2.5833283724514,330.812612550834));
#34947=CARTESIAN_POINT('Ctrl Pts',(89.5222510399454,-2.69872946464623,330.886027942706));
#34948=CARTESIAN_POINT('Ctrl Pts',(89.514475961167,-2.811011848806,330.964235456772));
#34949=CARTESIAN_POINT('Ctrl Pts',(89.506710450118,-2.92315606234381,331.042346731514));
#34950=CARTESIAN_POINT('Ctrl Pts',(89.498944939069,-3.03218888623276,331.125238173823));
#34951=CARTESIAN_POINT('Ctrl Pts',(89.49117942802,-3.13767809790927,331.212631623884));
#34952=CARTESIAN_POINT('Ctrl Pts',(89.4834216164978,-3.24306271672512,331.299938423086));
#34953=CARTESIAN_POINT('Ctrl Pts',(89.4756638049756,-3.34491041633648,331.39173809916));
#34954=CARTESIAN_POINT('Ctrl Pts',(89.4679059934534,-3.44281863968047,331.487709739106));
#34955=CARTESIAN_POINT('Ctrl Pts',(89.4601540199304,-3.54065318398155,331.583609157351));
#34956=CARTESIAN_POINT('Ctrl Pts',(89.4524020464075,-3.63455387485573,331.683674017863));
#34957=CARTESIAN_POINT('Ctrl Pts',(89.4446500728845,-3.72415217689618,331.7875439885));
#34958=CARTESIAN_POINT('Ctrl Pts',(89.4369013823268,-3.81371253400264,331.891369970144));
#34959=CARTESIAN_POINT('Ctrl Pts',(89.4291526917692,-3.8989738714565,331.998997561463));
#34960=CARTESIAN_POINT('Ctrl Pts',(89.4214040012116,-3.97960556103291,332.110030685094));
#34961=CARTESIAN_POINT('Ctrl Pts',(89.4136569228338,-4.06022047451285,332.221040707357));
#34962=CARTESIAN_POINT('Ctrl Pts',(89.4059098444559,-4.13620742652772,332.335454536501));
#34963=CARTESIAN_POINT('Ctrl Pts',(89.3981627660781,-4.20727728656692,332.452844548042));
#34964=CARTESIAN_POINT('Ctrl Pts',(89.3904156227723,-4.2783477422399,332.570235543425));
#34965=CARTESIAN_POINT('Ctrl Pts',(89.3826684794665,-4.34450082130757,332.690602436585));
#34966=CARTESIAN_POINT('Ctrl Pts',(89.3749213361608,-4.40549200327767,332.813490619376));
#34967=CARTESIAN_POINT('Ctrl Pts',(89.3671724511327,-4.46649689736039,332.936406430039));
#34968=CARTESIAN_POINT('Ctrl Pts',(89.3594235661046,-4.52233741133484,333.061844308225));
#34969=CARTESIAN_POINT('Ctrl Pts',(89.3516746810765,-4.57281623233117,333.189327537121));
#34970=CARTESIAN_POINT('Ctrl Pts',(89.3439175713018,-4.62334863206966,333.316946078033));
#34971=CARTESIAN_POINT('Ctrl Pts',(89.3361604615271,-4.66850782648172,333.44661394235));
#34972=CARTESIAN_POINT('Ctrl Pts',(89.3284033517524,-4.70814550215337,333.577836509731));
#34973=CARTESIAN_POINT('Ctrl Pts',(89.3206420968262,-4.74780435893156,333.709129198257));
#34974=CARTESIAN_POINT('Ctrl Pts',(89.3128808419,-4.78193572057139,333.841977866872));
#34975=CARTESIAN_POINT('Ctrl Pts',(89.3051195869739,-4.81044217368608,333.975876396072));
#34976=CARTESIAN_POINT('Ctrl Pts',(89.2973459165692,-4.83899422783549,334.109989119281));
#34977=CARTESIAN_POINT('Ctrl Pts',(89.2895722461646,-4.86190332739835,334.245154673503));
#34978=CARTESIAN_POINT('Ctrl Pts',(89.2817985757599,-4.87912371539755,334.380859602073));
#34979=CARTESIAN_POINT('Ctrl Pts',(89.2743867715828,-4.89554249019254,334.51024743357));
#34980=CARTESIAN_POINT('Ctrl Pts',(89.2669749674057,-4.90679022889298,334.640125267014));
#34981=CARTESIAN_POINT('Ctrl Pts',(89.2595631632285,-4.91287141281748,334.770048823398));
#34982=CARTESIAN_POINT('Ctrl Pts',(89.2552208583156,-4.91643415600394,334.846166281941));
#34983=CARTESIAN_POINT('Ctrl Pts',(89.2508785534028,-4.91822803246434,334.922367180039));
#34984=CARTESIAN_POINT('Ctrl Pts',(89.2465362484899,-4.91824979948594,334.998595593897));
#34985=CARTESIAN_POINT('',(92.7465362485305,-4.91824992232871,334.999125921265));
#34986=CARTESIAN_POINT('Ctrl Pts',(92.74653624849,-4.91824992232884,334.999125921985));
#34987=CARTESIAN_POINT('Ctrl Pts',(92.7385216442954,-4.9182752111004,335.141420427261));
#34988=CARTESIAN_POINT('Ctrl Pts',(92.7305070401008,-4.91212087654961,335.283631968748));
#34989=CARTESIAN_POINT('Ctrl Pts',(92.7224924359062,-4.899834566952,335.425210864163));
#34990=CARTESIAN_POINT('Ctrl Pts',(92.7144706815551,-4.8875372962347,335.566916067906));
#34991=CARTESIAN_POINT('Ctrl Pts',(92.706448927204,-4.86909717163168,335.70798715086));
#34992=CARTESIAN_POINT('Ctrl Pts',(92.698427172853,-4.84461342652192,335.847881955265));
#34993=CARTESIAN_POINT('Ctrl Pts',(92.6900932063248,-4.81917675727255,335.993221561334));
#34994=CARTESIAN_POINT('Ctrl Pts',(92.6817592397967,-4.78721663899655,336.137291062448));
#34995=CARTESIAN_POINT('Ctrl Pts',(92.6734252732686,-4.74890158037103,336.279498668405));
#34996=CARTESIAN_POINT('Ctrl Pts',(92.6653798140736,-4.71191292200677,336.41678329597));
#34997=CARTESIAN_POINT('Ctrl Pts',(92.6573343548786,-4.66900215389861,336.552332486576));
#34998=CARTESIAN_POINT('Ctrl Pts',(92.6492888956835,-4.62037042257736,336.68563347756));
#34999=CARTESIAN_POINT('Ctrl Pts',(92.6412347778026,-4.57168635280338,336.819077929767));
#35000=CARTESIAN_POINT('Ctrl Pts',(92.6331806599216,-4.51726917308143,336.950269033648));
#35001=CARTESIAN_POINT('Ctrl Pts',(92.6251265420407,-4.45736701682273,337.07871651262));
#35002=CARTESIAN_POINT('Ctrl Pts',(92.617057771837,-4.39735588454188,337.207397667577));
#35003=CARTESIAN_POINT('Ctrl Pts',(92.6089890016333,-4.33184000147973,337.333324915718));
#35004=CARTESIAN_POINT('Ctrl Pts',(92.6009202314296,-4.26111252886422,337.45603401419));
#35005=CARTESIAN_POINT('Ctrl Pts',(92.600086679125,-4.25380595719205,337.468710599251));
#35006=CARTESIAN_POINT('Ctrl Pts',(92.5992531268204,-4.24644380349574,337.481352867268));
#35007=CARTESIAN_POINT('Ctrl Pts',(92.5984195745157,-4.2390264160805,337.493960325721));
#35008=CARTESIAN_POINT('Ctrl Pts',(92.5906444957373,-4.16983967019412,337.611558204256));
#35009=CARTESIAN_POINT('Ctrl Pts',(92.5828694169588,-4.09564633712657,337.726460689746));
#35010=CARTESIAN_POINT('Ctrl Pts',(92.5750943381804,-4.01668206031312,337.838212164173));
#35011=CARTESIAN_POINT('Ctrl Pts',(92.5673288271314,-3.93781495406951,337.949826121296));
#35012=CARTESIAN_POINT('Ctrl Pts',(92.5595633160824,-3.85418880899566,338.058296466337));
#35013=CARTESIAN_POINT('Ctrl Pts',(92.5517978050334,-3.76608469852817,338.163192865763));
#35014=CARTESIAN_POINT('Ctrl Pts',(92.5440399935111,-3.67806794354261,338.267985260104));
#35015=CARTESIAN_POINT('Ctrl Pts',(92.5362821819889,-3.58558230861974,338.369210463371));
#35016=CARTESIAN_POINT('Ctrl Pts',(92.5285243704667,-3.48895141899565,338.466468095683));
#35017=CARTESIAN_POINT('Ctrl Pts',(92.5207723969437,-3.3923932471804,338.563652538543));
#35018=CARTESIAN_POINT('Ctrl Pts',(92.5130204234207,-3.29169630413375,338.656875077218));
#35019=CARTESIAN_POINT('Ctrl Pts',(92.5052684498977,-3.18722340349391,338.745769619013));
#35020=CARTESIAN_POINT('Ctrl Pts',(92.4975197593401,-3.08279474718951,338.834626513916));
#35021=CARTESIAN_POINT('Ctrl Pts',(92.4897710687824,-2.97459361090222,338.919158804691));
#35022=CARTESIAN_POINT('Ctrl Pts',(92.4820223782248,-2.86301829658375,338.999038546442));
#35023=CARTESIAN_POINT('Ctrl Pts',(92.474275299847,-2.75146619644132,339.078901668545));
#35024=CARTESIAN_POINT('Ctrl Pts',(92.4665282214691,-2.63654163226802,339.154113939655));
#35025=CARTESIAN_POINT('Ctrl Pts',(92.4587811430913,-2.5186741720712,339.224389124766));
#35026=CARTESIAN_POINT('Ctrl Pts',(92.4510339997855,-2.40080572403161,339.294664898851));
#35027=CARTESIAN_POINT('Ctrl Pts',(92.4432868564797,-2.27999466650391,339.360003304237));
#35028=CARTESIAN_POINT('Ctrl Pts',(92.4355397131739,-2.15669724917237,339.420162897215));
#35029=CARTESIAN_POINT('Ctrl Pts',(92.4277908281458,-2.0333721119639,339.480336015345));
#35030=CARTESIAN_POINT('Ctrl Pts',(92.4200419431176,-1.90755985385148,339.535327832858));
#35031=CARTESIAN_POINT('Ctrl Pts',(92.4122930580895,-1.7797385137572,339.584944261946));
#35032=CARTESIAN_POINT('Ctrl Pts',(92.4045359483148,-1.65178150277155,339.634613354424));
#35033=CARTESIAN_POINT('Ctrl Pts',(92.3967788385401,-1.52181151497495,339.678895519555));
#35034=CARTESIAN_POINT('Ctrl Pts',(92.3890217287654,-1.39032416138223,339.717645788821));
#35035=CARTESIAN_POINT('Ctrl Pts',(92.3812604738392,-1.25876654515208,339.756416764991));
#35036=CARTESIAN_POINT('Ctrl Pts',(92.373499218913,-1.12569032650598,339.789649860408));
#35037=CARTESIAN_POINT('Ctrl Pts',(92.3657379639868,-0.991602271494193,
339.817251083104));
#35038=CARTESIAN_POINT('Ctrl Pts',(92.3579642935822,-0.857299719293586,
339.844896458762));
#35039=CARTESIAN_POINT('Ctrl Pts',(92.3501906231775,-0.72198248228191,339.866891895982));
#35040=CARTESIAN_POINT('Ctrl Pts',(92.3424169527729,-0.586164314528041,
339.883195107599));
#35041=CARTESIAN_POINT('Ctrl Pts',(92.3350051485958,-0.456668515159256,
339.898739400792));
#35042=CARTESIAN_POINT('Ctrl Pts',(92.3275933444187,-0.326717659055883,
339.909109465582));
#35043=CARTESIAN_POINT('Ctrl Pts',(92.3201815402416,-0.196755984812248,
339.914312784606));
#35044=CARTESIAN_POINT('Ctrl Pts',(92.3124064614632,-0.0604245017779839,
339.919771133795));
#35045=CARTESIAN_POINT('Ctrl Pts',(92.3046313826847,0.0763497193427593,
339.919560705175));
#35046=CARTESIAN_POINT('Ctrl Pts',(92.2968563039063,0.213056019454141,339.913633095284));
#35047=CARTESIAN_POINT('Ctrl Pts',(92.2890907928573,0.3495940937599,339.907712779695));
#35048=CARTESIAN_POINT('Ctrl Pts',(92.2813252818083,0.486064026584502,339.896089297945));
#35049=CARTESIAN_POINT('Ctrl Pts',(92.2735597707593,0.621951836315044,339.878766132518));
#35050=CARTESIAN_POINT('Ctrl Pts',(92.2658019592371,0.757704912887165,339.86146014306));
#35051=CARTESIAN_POINT('Ctrl Pts',(92.2580441477149,0.892876629740933,339.838465765347));
#35052=CARTESIAN_POINT('Ctrl Pts',(92.2502863361926,1.0269551667081,339.809838474218));
#35053=CARTESIAN_POINT('Ctrl Pts',(92.2425343626696,1.16093280532377,339.781232726034));
#35054=CARTESIAN_POINT('Ctrl Pts',(92.2347823891467,1.29381852078329,339.747002583137));
#35055=CARTESIAN_POINT('Ctrl Pts',(92.2270304156237,1.42510811864993,339.70725502949));
#35056=CARTESIAN_POINT('Ctrl Pts',(92.219281725066,1.55634211529402,339.667524308956));
#35057=CARTESIAN_POINT('Ctrl Pts',(92.2115330345084,1.68598096544852,339.622280938082));
#35058=CARTESIAN_POINT('Ctrl Pts',(92.2037843439508,1.81353334921395,339.571682387676));
#35059=CARTESIAN_POINT('Ctrl Pts',(92.196037265573,1.9410591946406,339.521094364722));
#35060=CARTESIAN_POINT('Ctrl Pts',(92.1882901871952,2.06649907404425,339.465153522477));
#35061=CARTESIAN_POINT('Ctrl Pts',(92.1805431088173,2.18937982240547,339.404066195659));
#35062=CARTESIAN_POINT('Ctrl Pts',(92.1727959655115,2.31226160062556,339.34297835687));
#35063=CARTESIAN_POINT('Ctrl Pts',(92.1650488222057,2.4325838550137,339.276744121475));
#35064=CARTESIAN_POINT('Ctrl Pts',(92.1573016788999,2.54989664751896,339.205616500523));
#35065=CARTESIAN_POINT('Ctrl Pts',(92.1495527938718,2.66723581443075,339.134472888571));
#35066=CARTESIAN_POINT('Ctrl Pts',(92.1418039088437,2.78156383894635,339.058433904523));
#35067=CARTESIAN_POINT('Ctrl Pts',(92.1340550238156,2.89245881419868,338.977796509459));
#35068=CARTESIAN_POINT('Ctrl Pts',(92.1262979140409,3.0034714945235,338.89707352503));
#35069=CARTESIAN_POINT('Ctrl Pts',(92.1185408042661,3.11104352997321,338.811742609967));
#35070=CARTESIAN_POINT('Ctrl Pts',(92.1107836944914,3.21478480987089,338.72214208336));
#35071=CARTESIAN_POINT('Ctrl Pts',(92.1030224395653,3.31858152579155,338.632493677098));
#35072=CARTESIAN_POINT('Ctrl Pts',(92.0952611846391,3.4185431225455,338.538571380626));
#35073=CARTESIAN_POINT('Ctrl Pts',(92.0874999297129,3.51431632009507,338.440750479883));
#35074=CARTESIAN_POINT('Ctrl Pts',(92.0797262593083,3.61024272354825,338.342773097578));
#35075=CARTESIAN_POINT('Ctrl Pts',(92.0719525889036,3.70196707740749,338.240884939286));
#35076=CARTESIAN_POINT('Ctrl Pts',(92.0641789184989,3.78917579968558,338.135495147752));
#35077=CARTESIAN_POINT('Ctrl Pts',(92.0567671143219,3.87232493496041,338.035011276369));
#35078=CARTESIAN_POINT('Ctrl Pts',(92.0493553101448,3.95136920849405,337.931344666184));
#35079=CARTESIAN_POINT('Ctrl Pts',(92.0419435059677,4.02607450960209,337.824872936192));
#35080=CARTESIAN_POINT('Ctrl Pts',(92.0341684271893,4.10444134005321,337.713182709551));
#35081=CARTESIAN_POINT('Ctrl Pts',(92.0263933484108,4.17828076528896,337.598052474059));
#35082=CARTESIAN_POINT('Ctrl Pts',(92.0186182696323,4.24727573486787,337.479885459956));
#35083=CARTESIAN_POINT('Ctrl Pts',(92.0108527585833,4.31618580174423,337.361863857887));
#35084=CARTESIAN_POINT('Ctrl Pts',(92.0030872475343,4.38026307925953,337.240813246986));
#35085=CARTESIAN_POINT('Ctrl Pts',(91.9953217364853,4.43923235096435,337.117167729929));
#35086=CARTESIAN_POINT('Ctrl Pts',(91.9875639249631,4.49814315446468,336.993644807761));
#35087=CARTESIAN_POINT('Ctrl Pts',(91.9798061134409,4.55195586382368,336.867532450099));
#35088=CARTESIAN_POINT('Ctrl Pts',(91.9720483019187,4.60044015375487,336.73929107806));
#35089=CARTESIAN_POINT('Ctrl Pts',(91.9642963283957,4.64888795772016,336.611146211721));
#35090=CARTESIAN_POINT('Ctrl Pts',(91.9565443548727,4.6920151859054,336.480875884152));
#35091=CARTESIAN_POINT('Ctrl Pts',(91.9487923813497,4.72963895486805,336.348961978373));
#35092=CARTESIAN_POINT('Ctrl Pts',(91.9410436907921,4.76724679014225,336.217103938211));
#35093=CARTESIAN_POINT('Ctrl Pts',(91.9332950002345,4.79935569484358,336.083604079348));
#35094=CARTESIAN_POINT('Ctrl Pts',(91.9255463096768,4.82583220814465,335.94896077966));
#35095=CARTESIAN_POINT('Ctrl Pts',(91.917799231299,4.85230321278598,335.814345493636));
#35096=CARTESIAN_POINT('Ctrl Pts',(91.9100521529212,4.87314408158095,335.678587623279));
#35097=CARTESIAN_POINT('Ctrl Pts',(91.9023050745433,4.88827226905249,335.542196722705));
#35098=CARTESIAN_POINT('Ctrl Pts',(91.8945579312375,4.90340058331285,335.405804679044));
#35099=CARTESIAN_POINT('Ctrl Pts',(91.8868107879317,4.91281607766325,335.268779983074));
#35100=CARTESIAN_POINT('Ctrl Pts',(91.8790636446259,4.91648802719435,335.131637916098));
#35101=CARTESIAN_POINT('Ctrl Pts',(91.8713147595978,4.92016080225764,334.994465016674));
#35102=CARTESIAN_POINT('Ctrl Pts',(91.8635658745697,4.91808745255723,334.857175084394));
#35103=CARTESIAN_POINT('Ctrl Pts',(91.8558169895417,4.91028938098563,334.720283612422));
#35104=CARTESIAN_POINT('Ctrl Pts',(91.8480598797669,4.90248303246025,334.583246842427));
#35105=CARTESIAN_POINT('Ctrl Pts',(91.8403027699922,4.88893984639177,334.44660976844));
#35106=CARTESIAN_POINT('Ctrl Pts',(91.8325456602174,4.86973321125132,334.310883526727));
#35107=CARTESIAN_POINT('Ctrl Pts',(91.8247844052913,4.85051631269918,334.17508475725));
#35108=CARTESIAN_POINT('Ctrl Pts',(91.8170231503651,4.82563000565068,334.040198174072));
#35109=CARTESIAN_POINT('Ctrl Pts',(91.8092618954389,4.79519869595694,333.906723946666));
#35110=CARTESIAN_POINT('Ctrl Pts',(91.8014882250343,4.76471870608524,333.773036203996));
#35111=CARTESIAN_POINT('Ctrl Pts',(91.7937145546296,4.72867609110482,333.64076570919));
#35112=CARTESIAN_POINT('Ctrl Pts',(91.785940884225,4.68724521067128,333.510397570645));
#35113=CARTESIAN_POINT('Ctrl Pts',(91.7785290800479,4.64774294768982,333.386098100316));
#35114=CARTESIAN_POINT('Ctrl Pts',(91.7711172758708,4.60334287552367,333.263528133206));
#35115=CARTESIAN_POINT('Ctrl Pts',(91.7637054716938,4.55423585131794,333.143088889292));
#35116=CARTESIAN_POINT('Ctrl Pts',(91.7559303929154,4.50272194557331,333.016746559263));
#35117=CARTESIAN_POINT('Ctrl Pts',(91.7481553141369,4.44586522425323,332.892349834692));
#35118=CARTESIAN_POINT('Ctrl Pts',(91.7403802353585,4.38383319808107,332.770383541077));
#35119=CARTESIAN_POINT('Ctrl Pts',(91.7326147243095,4.32187750626643,332.648567334751));
#35120=CARTESIAN_POINT('Ctrl Pts',(91.7248492132605,4.25475935667564,332.529175953619));
#35121=CARTESIAN_POINT('Ctrl Pts',(91.7170837022115,4.18269486009623,332.41267575093));
#35122=CARTESIAN_POINT('Ctrl Pts',(91.7093258906893,4.11070181567483,332.296291058531));
#35123=CARTESIAN_POINT('Ctrl Pts',(91.7015680791671,4.0337723884349,332.182792170131));
#35124=CARTESIAN_POINT('Ctrl Pts',(91.6938102676449,3.95216911408752,332.072621931463));
#35125=CARTESIAN_POINT('Ctrl Pts',(91.6860582941219,3.87062724879194,331.962534599392));
#35126=CARTESIAN_POINT('Ctrl Pts',(91.6783063205989,3.78441876895418,331.855771243975));
#35127=CARTESIAN_POINT('Ctrl Pts',(91.6705543470759,3.69384993156173,331.75274643035));
#35128=CARTESIAN_POINT('Ctrl Pts',(91.6628056565183,3.6033194501257,331.649765247796));
#35129=CARTESIAN_POINT('Ctrl Pts',(91.6550569659607,3.50843254145613,331.550519750968));
#35130=CARTESIAN_POINT('Ctrl Pts',(91.647308275403,3.40953607882918,331.45539187079));
#35131=CARTESIAN_POINT('Ctrl Pts',(91.6395611970252,3.31066019243734,331.360283782761));
#35132=CARTESIAN_POINT('Ctrl Pts',(91.6318141186474,3.20777669294131,331.269291878137));
#35133=CARTESIAN_POINT('Ctrl Pts',(91.6240670402696,3.10126940517231,331.182761320137));
#35134=CARTESIAN_POINT('Ctrl Pts',(91.6163198969638,2.9947612247698,331.096230036928));
#35135=CARTESIAN_POINT('Ctrl Pts',(91.608572753658,2.88462949888965,331.014160421394));
#35136=CARTESIAN_POINT('Ctrl Pts',(91.6008256103522,2.7712909115599,330.936857159045));
#35137=CARTESIAN_POINT('Ctrl Pts',(91.5930767253241,2.65792684330955,330.859536517281));
#35138=CARTESIAN_POINT('Ctrl Pts',(91.585327840296,2.54135480181096,330.786984581226));
#35139=CARTESIAN_POINT('Ctrl Pts',(91.5775789552679,2.42201985859766,330.71946231566));
#35140=CARTESIAN_POINT('Ctrl Pts',(91.5698218454932,2.30255825204242,330.651868381263));
#35141=CARTESIAN_POINT('Ctrl Pts',(91.5620647357185,2.18032822641381,330.589314974392));
#35142=CARTESIAN_POINT('Ctrl Pts',(91.5543076259438,2.0557993218143,330.532016986276));
#35143=CARTESIAN_POINT('Ctrl Pts',(91.5465463710176,1.93120387294966,330.474688379947));
#35144=CARTESIAN_POINT('Ctrl Pts',(91.5387851160914,1.80430745875579,330.422620936522));
#35145=CARTESIAN_POINT('Ctrl Pts',(91.5310238611652,1.67559800555924,330.375980710868));
#35146=CARTESIAN_POINT('Ctrl Pts',(91.5232501907605,1.54668265918398,330.329265876053));
#35147=CARTESIAN_POINT('Ctrl Pts',(91.5154765203559,1.41594885114326,330.287995725506));
#35148=CARTESIAN_POINT('Ctrl Pts',(91.5077028499513,1.28389887545314,330.252286156463));
#35149=CARTESIAN_POINT('Ctrl Pts',(91.5002910457741,1.15799585790016,330.21823887645));
#35150=CARTESIAN_POINT('Ctrl Pts',(91.492879241597,1.03089673091616,330.189246202102));
#35151=CARTESIAN_POINT('Ctrl Pts',(91.4854674374199,0.903042172690774,330.165364760725));
#35152=CARTESIAN_POINT('Ctrl Pts',(91.4776923586414,0.768921081708359,330.140312818766));
#35153=CARTESIAN_POINT('Ctrl Pts',(91.469917279863,0.63354478778416,330.120806643161));
#35154=CARTESIAN_POINT('Ctrl Pts',(91.4621422010846,0.497411640688017,330.106967737465));
#35155=CARTESIAN_POINT('Ctrl Pts',(91.4543766900356,0.361446014095945,330.093145861423));
#35156=CARTESIAN_POINT('Ctrl Pts',(91.4466111789865,0.224725772616025,330.084977418311));
#35157=CARTESIAN_POINT('Ctrl Pts',(91.4388456679375,0.0877600325927998,
330.082533046458));
#35158=CARTESIAN_POINT('Ctrl Pts',(91.4310878564153,-0.0490699054997757,
330.080091098207));
#35159=CARTESIAN_POINT('Ctrl Pts',(91.4233300448932,-0.186144469436422,
330.083361933712));
#35160=CARTESIAN_POINT('Ctrl Pts',(91.415572233371,-0.322949187655547,330.09236443033));
#35161=CARTESIAN_POINT('Ctrl Pts',(91.407820259848,-0.459650955985886,330.101360152283));
#35162=CARTESIAN_POINT('Ctrl Pts',(91.4000682863251,-0.596082894334293,
330.116078924459));
#35163=CARTESIAN_POINT('Ctrl Pts',(91.3923163128021,-0.731730652800285,
330.136487553809));
#35164=CARTESIAN_POINT('Ctrl Pts',(91.3845676222444,-0.867320964360587,
330.156887540093));
#35165=CARTESIAN_POINT('Ctrl Pts',(91.3768189316868,-1.00212737084362,330.182972532877));
#35166=CARTESIAN_POINT('Ctrl Pts',(91.3690702411292,-1.1356409853554,330.214657523763));
#35167=CARTESIAN_POINT('Ctrl Pts',(91.3613231627513,-1.26912682124464,330.246335922321));
#35168=CARTESIAN_POINT('Ctrl Pts',(91.3535760843735,-1.40132002010244,330.283611911263));
#35169=CARTESIAN_POINT('Ctrl Pts',(91.3458290059957,-1.53172261717168,330.326349511726));
#35170=CARTESIAN_POINT('Ctrl Pts',(91.3380818626899,-1.66212630714002,330.36908747037));
#35171=CARTESIAN_POINT('Ctrl Pts',(91.3303347193841,-1.79073899395236,330.417287010101));
#35172=CARTESIAN_POINT('Ctrl Pts',(91.3225875760783,-1.9170789694255,330.470762615242));
#35173=CARTESIAN_POINT('Ctrl Pts',(91.3148386910501,-2.04344734880809,330.524250242835));
#35174=CARTESIAN_POINT('Ctrl Pts',(91.307089806022,-2.1675416402231,330.583016143858));
#35175=CARTESIAN_POINT('Ctrl Pts',(91.2993409209939,-2.28890153907308,330.646827271182));
#35176=CARTESIAN_POINT('Ctrl Pts',(91.2915838112191,-2.41039025057309,330.710706128294));
#35177=CARTESIAN_POINT('Ctrl Pts',(91.2838267014444,-2.5291384253549,330.779640726737));
#35178=CARTESIAN_POINT('Ctrl Pts',(91.2760695916697,-2.64471126170638,330.853352510195));
#35179=CARTESIAN_POINT('Ctrl Pts',(91.2683083367435,-2.7603458564859,330.927103682874));
#35180=CARTESIAN_POINT('Ctrl Pts',(91.2605470818174,-2.87280141150711,331.005636903518));
#35181=CARTESIAN_POINT('Ctrl Pts',(91.2527858268912,-2.9816742427561,331.08863172629));
#35182=CARTESIAN_POINT('Ctrl Pts',(91.2450121564865,-3.09072123505374,331.17175931373));
#35183=CARTESIAN_POINT('Ctrl Pts',(91.2372384860819,-3.19617375014363,331.259362515454));
#35184=CARTESIAN_POINT('Ctrl Pts',(91.2294648156772,-3.29766250745396,331.35108166035));
#35185=CARTESIAN_POINT('Ctrl Pts',(91.2220530115001,-3.39442693869492,331.438531256986));
#35186=CARTESIAN_POINT('Ctrl Pts',(91.214641207323,-3.48758812764284,331.529722024718));
#35187=CARTESIAN_POINT('Ctrl Pts',(91.2072294031459,-3.57685997893381,331.624314032141));
#35188=CARTESIAN_POINT('Ctrl Pts',(91.1995477071593,-3.66938255581156,331.722350492147));
#35189=CARTESIAN_POINT('Ctrl Pts',(91.1918660111727,-3.75803546327572,331.824367545194));
#35190=CARTESIAN_POINT('Ctrl Pts',(91.1841843151861,-3.84245036478083,331.930023085315));
#35191=CARTESIAN_POINT('Ctrl Pts',(91.1763656457404,-3.92837048089958,332.037562585024));
#35192=CARTESIAN_POINT('Ctrl Pts',(91.1685469762948,-4.00989966813559,332.148871329607));
#35193=CARTESIAN_POINT('Ctrl Pts',(91.1607283068491,-4.08668713848287,332.263547680909));
#35194=CARTESIAN_POINT('Ctrl Pts',(91.1530654938859,-4.16194393598232,332.375938086647));
#35195=CARTESIAN_POINT('Ctrl Pts',(91.1454026809227,-4.2326460286149,332.491562759607));
#35196=CARTESIAN_POINT('Ctrl Pts',(91.1377398679595,-4.29850296491242,332.610009346642));
#35197=CARTESIAN_POINT('Ctrl Pts',(91.1300820975968,-4.36431656331045,332.728377988564));
#35198=CARTESIAN_POINT('Ctrl Pts',(91.122424327234,-4.42529115152225,332.849564502683));
#35199=CARTESIAN_POINT('Ctrl Pts',(91.1147665568713,-4.48117994661044,332.973128186442));
#35200=CARTESIAN_POINT('Ctrl Pts',(91.1071120720526,-4.53704476277447,333.096638855563));
#35201=CARTESIAN_POINT('Ctrl Pts',(91.0994575872338,-4.58782796147704,333.222524300614));
#35202=CARTESIAN_POINT('Ctrl Pts',(91.0918031024151,-4.63332927429757,333.350320364908));
#35203=CARTESIAN_POINT('Ctrl Pts',(91.0838641979213,-4.68052129118407,333.482864980664));
#35204=CARTESIAN_POINT('Ctrl Pts',(91.0759252934276,-4.72203111363083,333.617464540475));
#35205=CARTESIAN_POINT('Ctrl Pts',(91.0679863889338,-4.75769068907947,333.753580179255));
#35206=CARTESIAN_POINT('Ctrl Pts',(91.0603311154467,-4.79207626491121,333.884832852913));
#35207=CARTESIAN_POINT('Ctrl Pts',(91.0526758419597,-4.82102236314032,334.017494719986));
#35208=CARTESIAN_POINT('Ctrl Pts',(91.0450205684727,-4.84442983550854,334.151069713501));
#35209=CARTESIAN_POINT('Ctrl Pts',(91.0373637237924,-4.86784211210249,334.284672122383));
#35210=CARTESIAN_POINT('Ctrl Pts',(91.0297068791121,-4.88571344104874,334.419187634097));
#35211=CARTESIAN_POINT('Ctrl Pts',(91.0220500344319,-4.89799632491054,334.554113171687));
#35212=CARTESIAN_POINT('Ctrl Pts',(91.0143877267148,-4.91028797241442,334.6891349765));
#35213=CARTESIAN_POINT('Ctrl Pts',(91.0067254189978,-4.91698319519118,334.824566991026));
#35214=CARTESIAN_POINT('Ctrl Pts',(90.9990631112807,-4.91808655900643,334.959904356592));
#35215=CARTESIAN_POINT('Ctrl Pts',(90.9982208236838,-4.91820784748646,334.974781465242));
#35216=CARTESIAN_POINT('Ctrl Pts',(90.9973785360868,-4.91826161713711,334.989657433038));
#35217=CARTESIAN_POINT('Ctrl Pts',(90.9965362484899,-4.91824791233352,335.004531592096));
#35218=CARTESIAN_POINT('',(94.4965362484452,-4.91824822735333,334.995824280208));
#35219=CARTESIAN_POINT('Ctrl Pts',(94.4965362484452,-4.91824822735333,334.995824280208));
#35220=CARTESIAN_POINT('Ctrl Pts',(94.4888886712765,-4.91836262203263,335.130560674578));
#35221=CARTESIAN_POINT('Ctrl Pts',(94.4812410941079,-4.91293616218613,335.26549038709));
#35222=CARTESIAN_POINT('Ctrl Pts',(94.4735935169392,-4.90194789488013,335.400112357195));
#35223=CARTESIAN_POINT('Ctrl Pts',(94.4659528995935,-4.89096962765567,335.534611812017));
#35224=CARTESIAN_POINT('Ctrl Pts',(94.4583122822477,-4.87443965323708,335.668803681708));
#35225=CARTESIAN_POINT('Ctrl Pts',(94.450671664902,-4.85238907099769,335.802186615547));
#35226=CARTESIAN_POINT('Ctrl Pts',(94.4430357359871,-4.83035201942287,335.935487703032));
#35227=CARTESIAN_POINT('Ctrl Pts',(94.4353998070723,-4.8028011628594,336.067980445035));
#35228=CARTESIAN_POINT('Ctrl Pts',(94.4277638781574,-4.76981941654863,336.199168793797));
#35229=CARTESIAN_POINT('Ctrl Pts',(94.4201303938493,-4.73684822918865,336.330315143226));
#35230=CARTESIAN_POINT('Ctrl Pts',(94.4124969095411,-4.69844970651333,336.460157538624));
#35231=CARTESIAN_POINT('Ctrl Pts',(94.4048634252329,-4.6547577374,336.588210775878));
#35232=CARTESIAN_POINT('Ctrl Pts',(94.39723061841,-4.61106964602646,336.71625264818));
#35233=CARTESIAN_POINT('Ctrl Pts',(94.3895978115871,-4.56208917268773,336.842505296178));
#35234=CARTESIAN_POINT('Ctrl Pts',(94.3819650047642,-4.5079997054631,336.966499864746));
#35235=CARTESIAN_POINT('Ctrl Pts',(94.3743311090654,-4.45390252197905,337.090512122048));
#35236=CARTESIAN_POINT('Ctrl Pts',(94.3666972133666,-4.39469505718639,337.212265289701));
#35237=CARTESIAN_POINT('Ctrl Pts',(94.3590633176678,-4.33060811467945,337.331312166908));
#35238=CARTESIAN_POINT('Ctrl Pts',(94.3514218949351,-4.26645798233973,337.450476424536));
#35239=CARTESIAN_POINT('Ctrl Pts',(94.3437804722023,-4.19741895439889,337.566928706103));
#35240=CARTESIAN_POINT('Ctrl Pts',(94.3361390494696,-4.12376710295986,337.680247739118));
#35241=CARTESIAN_POINT('Ctrl Pts',(94.3284938982079,-4.05007931409524,337.793622064623));
#35242=CARTESIAN_POINT('Ctrl Pts',(94.3208487469462,-3.97177445363895,337.90385976865));
#35243=CARTESIAN_POINT('Ctrl Pts',(94.3132035956845,-3.88917011445415,338.010571188884));
#35244=CARTESIAN_POINT('Ctrl Pts',(94.3055463263312,-3.8064348416994,338.117451754073));
#35245=CARTESIAN_POINT('Ctrl Pts',(94.2978890569779,-3.71938673538526,338.220794560457));
#35246=CARTESIAN_POINT('Ctrl Pts',(94.2902317876246,-3.62838208559448,338.320244946301));
#35247=CARTESIAN_POINT('Ctrl Pts',(94.2827704518028,-3.53970605474,338.417150604461));
#35248=CARTESIAN_POINT('Ctrl Pts',(94.275309115981,-3.44727379825481,338.510360436865));
#35249=CARTESIAN_POINT('Ctrl Pts',(94.2678477801592,-3.35144469859913,338.599583516844));
#35250=CARTESIAN_POINT('Ctrl Pts',(94.2600727013807,-3.2515860651206,338.69255835302));
#35251=CARTESIAN_POINT('Ctrl Pts',(94.2522976226023,-3.14769778161514,338.781521583591));
#35252=CARTESIAN_POINT('Ctrl Pts',(94.2445225438239,-3.04013567261027,338.866103743386));
#35253=CARTESIAN_POINT('Ctrl Pts',(94.2367570327749,-2.93270592562819,338.950581819449));
#35254=CARTESIAN_POINT('Ctrl Pts',(94.2289915217258,-2.82161165271248,339.030689312347));
#35255=CARTESIAN_POINT('Ctrl Pts',(94.2212260106768,-2.70724500788517,339.106093950433));
#35256=CARTESIAN_POINT('Ctrl Pts',(94.2134681991546,-2.59299175791934,339.1814238246));
#35257=CARTESIAN_POINT('Ctrl Pts',(94.2057103876325,-2.47547291713893,339.252059909607));
#35258=CARTESIAN_POINT('Ctrl Pts',(94.1979525761103,-2.3551128784969,339.317710781425));
#35259=CARTESIAN_POINT('Ctrl Pts',(94.1902006025873,-2.23484341460095,339.383312248881));
#35260=CARTESIAN_POINT('Ctrl Pts',(94.1824486290643,-2.11173735037519,339.443935783971));
#35261=CARTESIAN_POINT('Ctrl Pts',(94.1746966555413,-1.98624685785034,339.499334004292));
#35262=CARTESIAN_POINT('Ctrl Pts',(94.1669479649836,-1.86080951062341,339.554708763434));
#35263=CARTESIAN_POINT('Ctrl Pts',(94.159199274426,-1.73299010036903,339.60486245163));
#35264=CARTESIAN_POINT('Ctrl Pts',(94.1514505838684,-1.60326393054789,339.649594372793));
#35265=CARTESIAN_POINT('Ctrl Pts',(94.1437035054906,-1.47356475133979,339.694316987105));
#35266=CARTESIAN_POINT('Ctrl Pts',(94.1359564271127,-1.3419599709547,339.733619950806));
#35267=CARTESIAN_POINT('Ctrl Pts',(94.1282093487349,-1.20894296132336,339.767351463734));
#35268=CARTESIAN_POINT('Ctrl Pts',(94.1204622054291,-1.07592483688136,339.801083259364));
#35269=CARTESIAN_POINT('Ctrl Pts',(94.1127150621233,-0.941494838467383,
339.829243415007));
#35270=CARTESIAN_POINT('Ctrl Pts',(94.1049679188175,-0.80615913357158,339.851730672024));
#35271=CARTESIAN_POINT('Ctrl Pts',(94.0972190337894,-0.670793002336426,
339.874222984654));
#35272=CARTESIAN_POINT('Ctrl Pts',(94.0894701487613,-0.534521144946693,
339.891039796723));
#35273=CARTESIAN_POINT('Ctrl Pts',(94.0817212637332,-0.397857103704945,
339.902131453514));
#35274=CARTESIAN_POINT('Ctrl Pts',(94.0739641539585,-0.26104800583754,339.913234883105));
#35275=CARTESIAN_POINT('Ctrl Pts',(94.0662070441838,-0.123846282792389,
339.918600986893));
#35276=CARTESIAN_POINT('Ctrl Pts',(94.058449934409,0.0132316932650192,339.918232201187));
#35277=CARTESIAN_POINT('Ctrl Pts',(94.0506886794829,0.150382919409742,339.917863218414));
#35278=CARTESIAN_POINT('Ctrl Pts',(94.0429274245567,0.287409876515621,339.911753257175));
#35279=CARTESIAN_POINT('Ctrl Pts',(94.0351661696306,0.423800042786107,339.899956794323));
#35280=CARTESIAN_POINT('Ctrl Pts',(94.0273924992259,0.560408388873267,339.888141460975));
#35281=CARTESIAN_POINT('Ctrl Pts',(94.0196188288213,0.696377520671859,339.870621498393));
#35282=CARTESIAN_POINT('Ctrl Pts',(94.0118451584166,0.831202968369057,339.847502933251));
#35283=CARTESIAN_POINT('Ctrl Pts',(94.0044333542395,0.959752259039186,339.825460542878));
#35284=CARTESIAN_POINT('Ctrl Pts',(93.9970215500624,1.08726166490504,339.798329109787));
#35285=CARTESIAN_POINT('Ctrl Pts',(93.9896097458853,1.21330754079101,339.766242532012));
#35286=CARTESIAN_POINT('Ctrl Pts',(93.9818346671069,1.34553130052533,339.732583295479));
#35287=CARTESIAN_POINT('Ctrl Pts',(93.9740595883284,1.47656229037344,339.693364530291));
#35288=CARTESIAN_POINT('Ctrl Pts',(93.96628450955,1.60589726212151,339.64868551808));
#35289=CARTESIAN_POINT('Ctrl Pts',(93.9585189985009,1.73507307895307,339.604061486238));
#35290=CARTESIAN_POINT('Ctrl Pts',(93.9507534874519,1.86255666441301,339.553990703026));
#35291=CARTESIAN_POINT('Ctrl Pts',(93.9429879764029,1.98785638713942,339.49862312787));
#35292=CARTESIAN_POINT('Ctrl Pts',(93.9352301648807,2.11303187482587,339.443310449827));
#35293=CARTESIAN_POINT('Ctrl Pts',(93.9274723533585,2.23602745363899,339.382711588155));
#35294=CARTESIAN_POINT('Ctrl Pts',(93.9197145418363,2.35636839551839,339.317025717679));
#35295=CARTESIAN_POINT('Ctrl Pts',(93.9119625683133,2.47661877702239,339.251389277904));
#35296=CARTESIAN_POINT('Ctrl Pts',(93.9042105947903,2.59421815620286,339.180673635559));
#35297=CARTESIAN_POINT('Ctrl Pts',(93.8964586212673,2.70871380768813,339.105125158937));
#35298=CARTESIAN_POINT('Ctrl Pts',(93.8887099307097,2.82316097019724,339.02960867714));
#35299=CARTESIAN_POINT('Ctrl Pts',(93.880961240152,2.93450669374803,338.949263646651));
#35300=CARTESIAN_POINT('Ctrl Pts',(93.8732125495944,3.04232499474377,338.86438115212));
#35301=CARTESIAN_POINT('Ctrl Pts',(93.8654654712166,3.15012086324154,338.779516318101));
#35302=CARTESIAN_POINT('Ctrl Pts',(93.8577183928387,3.25439046205659,338.690116139472));
#35303=CARTESIAN_POINT('Ctrl Pts',(93.8499713144609,3.35473914733377,338.596513355438));
#35304=CARTESIAN_POINT('Ctrl Pts',(93.8422241711551,3.45508867362944,338.502909786923));
#35305=CARTESIAN_POINT('Ctrl Pts',(93.8344770278493,3.55151693501322,338.405103809366));
#35306=CARTESIAN_POINT('Ctrl Pts',(93.8267298845435,3.64366486466372,338.30346627295));
#35307=CARTESIAN_POINT('Ctrl Pts',(93.8189809995154,3.73583351112517,338.201805886257));
#35308=CARTESIAN_POINT('Ctrl Pts',(93.8112321144873,3.8237196484758,338.096312516103));
#35309=CARTESIAN_POINT('Ctrl Pts',(93.8034832294592,3.90700361379893,337.987391140153));
#35310=CARTESIAN_POINT('Ctrl Pts',(93.7957261196845,3.9903759775834,337.878354153928));
#35311=CARTESIAN_POINT('Ctrl Pts',(93.7879690099097,4.06913617371249,337.765882204615));
#35312=CARTESIAN_POINT('Ctrl Pts',(93.780211900135,4.14300681232222,337.650410839012));
#35313=CARTESIAN_POINT('Ctrl Pts',(93.7724506452088,4.21691692503935,337.534877769203));
#35314=CARTESIAN_POINT('Ctrl Pts',(93.7646893902826,4.28593207737853,337.416342427014));
#35315=CARTESIAN_POINT('Ctrl Pts',(93.7569281353565,4.34982072513485,337.29526528351));
#35316=CARTESIAN_POINT('Ctrl Pts',(93.7491544649518,4.41381157390618,337.173994456036));
#35317=CARTESIAN_POINT('Ctrl Pts',(93.7413807945471,4.47265936272183,337.050174055283));
#35318=CARTESIAN_POINT('Ctrl Pts',(93.7336071241425,4.52618025411252,336.924285677799));
#35319=CARTESIAN_POINT('Ctrl Pts',(93.7261953199655,4.57720973513215,336.804257434574));
#35320=CARTESIAN_POINT('Ctrl Pts',(93.7187835157884,4.62339699022363,336.682349679642));
#35321=CARTESIAN_POINT('Ctrl Pts',(93.7113717116114,4.66462535838777,336.558991125179));
#35322=CARTESIAN_POINT('Ctrl Pts',(93.703596632833,4.707874451689,336.429586400494));
#35323=CARTESIAN_POINT('Ctrl Pts',(93.6958215540545,4.74580294251021,336.298176121491));
#35324=CARTESIAN_POINT('Ctrl Pts',(93.6880464752761,4.77822198240916,336.16523720732));
#35325=CARTESIAN_POINT('Ctrl Pts',(93.6802809642271,4.81060112861556,336.032461882945));
#35326=CARTESIAN_POINT('Ctrl Pts',(93.6725154531781,4.83748422189758,335.898162042332));
#35327=CARTESIAN_POINT('Ctrl Pts',(93.6647499421291,4.85873131639776,335.762832260432));
#35328=CARTESIAN_POINT('Ctrl Pts',(93.6569921306069,4.87995734434189,335.627636658405));
#35329=CARTESIAN_POINT('Ctrl Pts',(93.6492343190848,4.89555843392246,335.491413530973));
#35330=CARTESIAN_POINT('Ctrl Pts',(93.6414765075626,4.9054451729057,335.354669872016));
#35331=CARTESIAN_POINT('Ctrl Pts',(93.6337245340396,4.91532447180431,335.218029117));
#35332=CARTESIAN_POINT('Ctrl Pts',(93.6259725605165,4.91949795142964,335.080868998439));
#35333=CARTESIAN_POINT('Ctrl Pts',(93.6182205869935,4.9179277924604,334.943703546777));
#35334=CARTESIAN_POINT('Ctrl Pts',(93.6104718964359,4.91635829845442,334.806596184764));
#35335=CARTESIAN_POINT('Ctrl Pts',(93.6027232058783,4.90905000825922,334.669483884179));
#35336=CARTESIAN_POINT('Ctrl Pts',(93.5949745153207,4.89601717700128,334.532882386322));
#35337=CARTESIAN_POINT('Ctrl Pts',(93.5872274369429,4.88298705733276,334.396309309548));
#35338=CARTESIAN_POINT('Ctrl Pts',(93.579480358565,4.864234802762,334.260247212973));
#35339=CARTESIAN_POINT('Ctrl Pts',(93.5717332801872,4.83982665635039,334.125208025311));
#35340=CARTESIAN_POINT('Ctrl Pts',(93.5639861368814,4.81541830537501,333.990167705891));
#35341=CARTESIAN_POINT('Ctrl Pts',(93.5562389935757,4.78535403753573,333.856150697125));
#35342=CARTESIAN_POINT('Ctrl Pts',(93.5484918502699,4.74975139700213,333.723659634276));
#35343=CARTESIAN_POINT('Ctrl Pts',(93.5407429652418,4.71414075223912,333.591138784624));
#35344=CARTESIAN_POINT('Ctrl Pts',(93.5329940802137,4.6729893585012,333.460144940959));
#35345=CARTESIAN_POINT('Ctrl Pts',(93.5252451951856,4.62646478219798,333.3311660713));
#35346=CARTESIAN_POINT('Ctrl Pts',(93.5174880854109,4.57989082422868,333.202050302135));
#35347=CARTESIAN_POINT('Ctrl Pts',(93.5097309756361,4.52793242395274,333.074954147523));
#35348=CARTESIAN_POINT('Ctrl Pts',(93.5019738658614,4.47080573039162,332.950346569881));
#35349=CARTESIAN_POINT('Ctrl Pts',(93.4942126109352,4.41364851015185,332.825672405934));
#35350=CARTESIAN_POINT('Ctrl Pts',(93.4864513560091,4.35131767108438,332.703489816744));
#35351=CARTESIAN_POINT('Ctrl Pts',(93.4786901010829,4.28407513127517,332.584242700086));
#35352=CARTESIAN_POINT('Ctrl Pts',(93.4709164306782,4.21672502531679,332.464804826904));
#35353=CARTESIAN_POINT('Ctrl Pts',(93.4631427602736,4.14444772394551,332.348312142166));
#35354=CARTESIAN_POINT('Ctrl Pts',(93.4553690898689,4.06754872696771,332.235179858247));
#35355=CARTESIAN_POINT('Ctrl Pts',(93.4479572856918,3.99422939679938,332.127313909361));
#35356=CARTESIAN_POINT('Ctrl Pts',(93.4405454815146,3.91670913884197,332.022502779932));
#35357=CARTESIAN_POINT('Ctrl Pts',(93.4331336773375,3.83528533434979,331.92107657344));
#35358=CARTESIAN_POINT('Ctrl Pts',(93.425358598559,3.74987070665105,331.814679166435));
#35359=CARTESIAN_POINT('Ctrl Pts',(93.4175835197806,3.65989028224242,331.711670647046));
#35360=CARTESIAN_POINT('Ctrl Pts',(93.4098084410021,3.56564291588129,331.612467910274));
#35361=CARTESIAN_POINT('Ctrl Pts',(93.4020429299531,3.47151152690454,331.513387248784));
#35362=CARTESIAN_POINT('Ctrl Pts',(93.3942774189041,3.3731239100977,331.418103332239));
#35363=CARTESIAN_POINT('Ctrl Pts',(93.3865119078551,3.27082023135558,331.327001486979));
#35364=CARTESIAN_POINT('Ctrl Pts',(93.3787540963329,3.16861798700885,331.235989969464));
#35365=CARTESIAN_POINT('Ctrl Pts',(93.3709962848106,3.06250769772058,331.149152529666));
#35366=CARTESIAN_POINT('Ctrl Pts',(93.3632384732884,2.95286731937084,331.06683871972));
#35367=CARTESIAN_POINT('Ctrl Pts',(93.3554864997654,2.84330944888308,330.984586853527));
#35368=CARTESIAN_POINT('Ctrl Pts',(93.3477345262425,2.73022708830162,330.906852075073));
#35369=CARTESIAN_POINT('Ctrl Pts',(93.3399825527195,2.61403203058852,330.833944358802));
#35370=CARTESIAN_POINT('Ctrl Pts',(93.3322338621619,2.49788618155103,330.761067518992));
#35371=CARTESIAN_POINT('Ctrl Pts',(93.3244851716042,2.37863058765178,330.693013882784));
#35372=CARTESIAN_POINT('Ctrl Pts',(93.3167364810466,2.25670666102128,330.630050559949));
#35373=CARTESIAN_POINT('Ctrl Pts',(93.3089894026688,2.13480810168196,330.56710033716));
#35374=CARTESIAN_POINT('Ctrl Pts',(93.3012423242909,2.01024266096208,330.509238500392));
#35375=CARTESIAN_POINT('Ctrl Pts',(93.2934952459131,1.88347667855987,330.456686378443));
#35376=CARTESIAN_POINT('Ctrl Pts',(93.2857481026073,1.7567096337368,330.404133816058));
#35377=CARTESIAN_POINT('Ctrl Pts',(93.2780009593015,1.62774237152265,330.356891206939));
#35378=CARTESIAN_POINT('Ctrl Pts',(93.2702538159957,1.49706117852844,330.31513171047));
#35379=CARTESIAN_POINT('Ctrl Pts',(93.2625049309676,1.36635060562787,330.27336282558));
#35380=CARTESIAN_POINT('Ctrl Pts',(93.2547560459395,1.23392570744121,330.237079625268));
#35381=CARTESIAN_POINT('Ctrl Pts',(93.2470071609114,1.10028750648357,330.206405266861));
#35382=CARTESIAN_POINT('Ctrl Pts',(93.2392500511367,0.966507460558331,330.175698350373));
#35383=CARTESIAN_POINT('Ctrl Pts',(93.2314929413619,0.831511920905739,330.150612255613));
#35384=CARTESIAN_POINT('Ctrl Pts',(93.2237358315872,0.695812218666052,330.13121900073));
#35385=CARTESIAN_POINT('Ctrl Pts',(93.215974576661,0.560040002844047,330.111815382711));
#35386=CARTESIAN_POINT('Ctrl Pts',(93.2082133217349,0.423563263380268,330.098110705207));
#35387=CARTESIAN_POINT('Ctrl Pts',(93.2004520668087,0.286897022290014,330.090124934268));
#35388=CARTESIAN_POINT('Ctrl Pts',(93.192678396404,0.150012159753719,330.082126388697));
#35389=CARTESIAN_POINT('Ctrl Pts',(93.1849047259994,0.0129375808524576,
330.079865037328));
#35390=CARTESIAN_POINT('Ctrl Pts',(93.1771310555947,-0.123812229994912,
330.083308674098));
#35391=CARTESIAN_POINT('Ctrl Pts',(93.1697192514176,-0.254196304247234,
330.086592008747));
#35392=CARTESIAN_POINT('Ctrl Pts',(93.1623074472405,-0.384284878722951,
330.09506113129));
#35393=CARTESIAN_POINT('Ctrl Pts',(93.1548956430634,-0.513639432302017,
330.10864460542));
#35394=CARTESIAN_POINT('Ctrl Pts',(93.147120564285,-0.649334037879509,330.122893846081));
#35395=CARTESIAN_POINT('Ctrl Pts',(93.1393454855065,-0.784649670147129,
330.142816484146));
#35396=CARTESIAN_POINT('Ctrl Pts',(93.1315704067281,-0.919074025747627,
330.168386812079));
#35397=CARTESIAN_POINT('Ctrl Pts',(93.1238048956791,-1.05333296362087,330.193925674095));
#35398=CARTESIAN_POINT('Ctrl Pts',(93.1160393846301,-1.18670242677202,330.225098325443));
#35399=CARTESIAN_POINT('Ctrl Pts',(93.108273873581,-1.31867430277485,330.261827235558));
#35400=CARTESIAN_POINT('Ctrl Pts',(93.1005160620588,-1.45051532827795,330.298519728851));
#35401=CARTESIAN_POINT('Ctrl Pts',(93.0927582505366,-1.58096115014035,330.340757413472));
#35402=CARTESIAN_POINT('Ctrl Pts',(93.0850004390145,-1.70951328890067,330.388411620973));
#35403=CARTESIAN_POINT('Ctrl Pts',(93.0772484654914,-1.83796868810056,330.436029967173));
#35404=CARTESIAN_POINT('Ctrl Pts',(93.0694964919684,-1.96453287567694,330.489056587651));
#35405=CARTESIAN_POINT('Ctrl Pts',(93.0617445184454,-2.08872234270765,330.547312941877));
#35406=CARTESIAN_POINT('Ctrl Pts',(93.0539958278878,-2.21285921542484,330.605544624502));
#35407=CARTESIAN_POINT('Ctrl Pts',(93.0462471373301,-2.33462301471646,330.66900147015));
#35408=CARTESIAN_POINT('Ctrl Pts',(93.0384984467725,-2.45355024884488,330.737456834366));
#35409=CARTESIAN_POINT('Ctrl Pts',(93.0307513683947,-2.57245273916926,330.805897955872));
#35410=CARTESIAN_POINT('Ctrl Pts',(93.0230042900168,-2.68851949967266,330.879335332474));
#35411=CARTESIAN_POINT('Ctrl Pts',(93.015257211639,-2.8013120470779,330.957496582884));
#35412=CARTESIAN_POINT('Ctrl Pts',(93.0075100683331,-2.91410553979324,331.03565848836));
#35413=CARTESIAN_POINT('Ctrl Pts',(92.9997629250273,-3.02362444340221,331.118544123978));
#35414=CARTESIAN_POINT('Ctrl Pts',(92.9920157817215,-3.12945998689764,331.205838267429));
#35415=CARTESIAN_POINT('Ctrl Pts',(92.9842668966934,-3.23531932446999,331.293152036457));
#35416=CARTESIAN_POINT('Ctrl Pts',(92.9765180116653,-3.33749335262792,331.384876036886));
#35417=CARTESIAN_POINT('Ctrl Pts',(92.9687691266372,-3.43560737371789,331.480655595689));
#35418=CARTESIAN_POINT('Ctrl Pts',(92.9610120168625,-3.53382553404348,331.576536815906));
#35419=CARTESIAN_POINT('Ctrl Pts',(92.9532549070878,-3.62797479886419,331.676481919888));
#35420=CARTESIAN_POINT('Ctrl Pts',(92.9454977973131,-3.71771789596114,331.780099891526));
#35421=CARTESIAN_POINT('Ctrl Pts',(92.9377365423869,-3.80750894889958,331.883773233295));
#35422=CARTESIAN_POINT('Ctrl Pts',(92.9299752874608,-3.89288889934658,331.991123047741));
#35423=CARTESIAN_POINT('Ctrl Pts',(92.9222140325346,-3.97356224945927,332.101727046641));
#35424=CARTESIAN_POINT('Ctrl Pts',(92.91444036213,-4.05436465064087,332.212507975894));
#35425=CARTESIAN_POINT('Ctrl Pts',(92.9066666917253,-4.13044518923159,332.326553166668));
#35426=CARTESIAN_POINT('Ctrl Pts',(92.8988930213207,-4.20155253095749,332.44341254949));
#35427=CARTESIAN_POINT('Ctrl Pts',(92.8914812171437,-4.26934980881759,332.554832099926));
#35428=CARTESIAN_POINT('Ctrl Pts',(92.8840694129667,-4.33262633511903,332.668809485685));
#35429=CARTESIAN_POINT('Ctrl Pts',(92.8766576087897,-4.39120487323533,332.784937286718));
#35430=CARTESIAN_POINT('Ctrl Pts',(92.8683539196665,-4.45683234506283,332.915039099356));
#35431=CARTESIAN_POINT('Ctrl Pts',(92.8600502305431,-4.51674859593692,333.048207284752));
#35432=CARTESIAN_POINT('Ctrl Pts',(92.8517465414198,-4.57067641724909,333.183932778969));
#35433=CARTESIAN_POINT('Ctrl Pts',(92.8434591402355,-4.6244984574984,333.319392043498));
#35434=CARTESIAN_POINT('Ctrl Pts',(92.8351717390511,-4.67235536885029,333.457398331321));
#35435=CARTESIAN_POINT('Ctrl Pts',(92.8268843378668,-4.71401640749578,333.597419388284));
#35436=CARTESIAN_POINT('Ctrl Pts',(92.8186195205387,-4.75556391635215,333.737058876242));
#35437=CARTESIAN_POINT('Ctrl Pts',(92.8103547032106,-4.79094913653858,333.878701887954));
#35438=CARTESIAN_POINT('Ctrl Pts',(92.8020898858825,-4.81999013535232,334.021798508687));
#35439=CARTESIAN_POINT('Ctrl Pts',(92.793839113524,-4.84898178280976,334.164651955542));
#35440=CARTESIAN_POINT('Ctrl Pts',(92.7855883411655,-4.87165063190238,334.308953787067));
#35441=CARTESIAN_POINT('Ctrl Pts',(92.777337568807,-4.88786446438492,334.454139174969));
#35442=CARTESIAN_POINT('Ctrl Pts',(92.7691055753873,-4.90404139382923,334.598994117746));
#35443=CARTESIAN_POINT('Ctrl Pts',(92.7608735819676,-4.91379256717959,334.744728300258));
#35444=CARTESIAN_POINT('Ctrl Pts',(92.7526415885479,-4.91703684368418,334.890767494067));
#35445=CARTESIAN_POINT('Ctrl Pts',(92.7506064752088,-4.91783889369244,334.926871302246));
#35446=CARTESIAN_POINT('Ctrl Pts',(92.7485713618697,-4.91824350085643,334.962993700791));
#35447=CARTESIAN_POINT('Ctrl Pts',(92.7465362485306,-4.91824992232871,334.999125921265));
#35448=CARTESIAN_POINT('',(96.2465362485274,-4.91824904506439,335.003064836579));
#35449=CARTESIAN_POINT('Ctrl Pts',(96.2465362484899,-4.91824904506398,335.003064837238));
#35450=CARTESIAN_POINT('Ctrl Pts',(96.2361955056856,-4.91813576058702,335.184856308468));
#35451=CARTESIAN_POINT('Ctrl Pts',(96.2258547628812,-4.90794384176267,335.366332575828));
#35452=CARTESIAN_POINT('Ctrl Pts',(96.2155140200769,-4.88777377337727,335.546672299267));
#35453=CARTESIAN_POINT('Ctrl Pts',(96.2077389412984,-4.87260814421216,335.682267544516));
#35454=CARTESIAN_POINT('Ctrl Pts',(96.19996386252,-4.85177180734536,335.817445497264));
#35455=CARTESIAN_POINT('Ctrl Pts',(96.1921887837416,-4.82529393069937,335.951694039519));
#35456=CARTESIAN_POINT('Ctrl Pts',(96.1844232726926,-4.7988486367663,336.085777380395));
#35457=CARTESIAN_POINT('Ctrl Pts',(96.1766577616436,-4.76677569110059,336.218933206589));
#35458=CARTESIAN_POINT('Ctrl Pts',(96.1688922505946,-4.72915605515843,336.350653941044));
#35459=CARTESIAN_POINT('Ctrl Pts',(96.1611344390724,-4.69157371919482,336.482244074007));
#35460=CARTESIAN_POINT('Ctrl Pts',(96.1533766275502,-4.64845574403999,336.612401573453));
#35461=CARTESIAN_POINT('Ctrl Pts',(96.145618816028,-4.59993416278677,336.740628840542));
#35462=CARTESIAN_POINT('Ctrl Pts',(96.137866842505,-4.55144909556219,336.868759612546));
#35463=CARTESIAN_POINT('Ctrl Pts',(96.130114868982,-4.49756865395786,336.994962679341));
#35464=CARTESIAN_POINT('Ctrl Pts',(96.122362895459,-4.43847464087635,337.118755749207));
#35465=CARTESIAN_POINT('Ctrl Pts',(96.1146142049014,-4.37940565414439,337.242496392634));
#35466=CARTESIAN_POINT('Ctrl Pts',(96.1068655143438,-4.31512765542954,337.363828717093));
#35467=CARTESIAN_POINT('Ctrl Pts',(96.0991168237861,-4.24587041522989,337.482290772568));
#35468=CARTESIAN_POINT('Ctrl Pts',(96.0913697454083,-4.17662758457751,337.600728181022));
#35469=CARTESIAN_POINT('Ctrl Pts',(96.0836226670305,-4.10240777021781,337.716296171107));
#35470=CARTESIAN_POINT('Ctrl Pts',(96.0758755886527,-4.02348630949061,337.828558109681));
#35471=CARTESIAN_POINT('Ctrl Pts',(96.0681284453469,-3.94456418732567,337.940820989118));
#35472=CARTESIAN_POINT('Ctrl Pts',(96.0603813020411,-3.86094056499591,338.049777442014));
#35473=CARTESIAN_POINT('Ctrl Pts',(96.0526341587353,-3.77293341915518,338.155020836242));
#35474=CARTESIAN_POINT('Ctrl Pts',(96.0448852737072,-3.68490648743968,338.26028789142));
#35475=CARTESIAN_POINT('Ctrl Pts',(96.0371363886791,-3.59249432185405,338.361839927029));
#35476=CARTESIAN_POINT('Ctrl Pts',(96.0293875036511,-3.49605411868056,338.459304650035));
#35477=CARTESIAN_POINT('Ctrl Pts',(96.0216303938763,-3.39951155287887,338.556872823106));
#35478=CARTESIAN_POINT('Ctrl Pts',(96.0138732841016,-3.2989326843352,338.650344739096));
#35479=CARTESIAN_POINT('Ctrl Pts',(96.0061161743269,-3.19471079875179,338.739385775076));
#35480=CARTESIAN_POINT('Ctrl Pts',(95.9983549194007,-3.09043322032509,338.828474391738));
#35481=CARTESIAN_POINT('Ctrl Pts',(95.9905936644746,-2.98250905325593,338.91312716938));
#35482=CARTESIAN_POINT('Ctrl Pts',(95.9828324095484,-2.87136257243016,338.993051469759));
#35483=CARTESIAN_POINT('Ctrl Pts',(95.9750587391437,-2.76003829345763,339.073103622972));
#35484=CARTESIAN_POINT('Ctrl Pts',(95.9672850687391,-2.64548172699808,339.148411968937));
#35485=CARTESIAN_POINT('Ctrl Pts',(95.9595113983344,-2.5281446301959,339.218728219655));
#35486=CARTESIAN_POINT('Ctrl Pts',(95.9520995941572,-2.41626960347716,339.285771231986));
#35487=CARTESIAN_POINT('Ctrl Pts',(95.94468778998,-2.30186734070033,339.348276315923));
#35488=CARTESIAN_POINT('Ctrl Pts',(95.9372759858027,-2.18534644997726,339.406068991297));
#35489=CARTESIAN_POINT('Ctrl Pts',(95.9295009070243,-2.06311452330447,339.466694257846));
#35490=CARTESIAN_POINT('Ctrl Pts',(95.9217258282459,-1.93816476147536,339.522325084392));
#35491=CARTESIAN_POINT('Ctrl Pts',(95.9139507494674,-1.81094359987295,339.572708862434));
#35492=CARTESIAN_POINT('Ctrl Pts',(95.9061852384184,-1.68387899200919,339.623030640028));
#35493=CARTESIAN_POINT('Ctrl Pts',(95.8984197273694,-1.55454890576231,339.668118073805));
#35494=CARTESIAN_POINT('Ctrl Pts',(95.8906542163204,-1.42342398639763,339.707764566909));
#35495=CARTESIAN_POINT('Ctrl Pts',(95.8828964047982,-1.29242907777226,339.7473717504));
#35496=CARTESIAN_POINT('Ctrl Pts',(95.875138593276,-1.15964324923439,339.781548616597));
#35497=CARTESIAN_POINT('Ctrl Pts',(95.8673807817538,-1.02555639294622,339.810136915659));
#35498=CARTESIAN_POINT('Ctrl Pts',(95.8596288082308,-0.891570441269536,
339.83870370112));
#35499=CARTESIAN_POINT('Ctrl Pts',(95.8518768347078,-0.756285791365676,
339.861690209259));
#35500=CARTESIAN_POINT('Ctrl Pts',(95.8441248611848,-0.620206396613705,
339.878988326293));
#35501=CARTESIAN_POINT('Ctrl Pts',(95.8363761706271,-0.484184631566295,
339.896279117563));
#35502=CARTESIAN_POINT('Ctrl Pts',(95.8286274800695,-0.347369178041581,
339.907886259945));
#35503=CARTESIAN_POINT('Ctrl Pts',(95.8208787895119,-0.210272841664043,
339.913752984691));
#35504=CARTESIAN_POINT('Ctrl Pts',(95.8131317111341,-0.0732050293243404,
339.919618488816));
#35505=CARTESIAN_POINT('Ctrl Pts',(95.8053846327563,0.0641431593551316,
339.919745934235));
#35506=CARTESIAN_POINT('Ctrl Pts',(95.7976375543785,0.201255549417171,339.914130570745));
#35507=CARTESIAN_POINT('Ctrl Pts',(95.7898904110726,0.338369088613009,339.908515160192));
#35508=CARTESIAN_POINT('Ctrl Pts',(95.7821432677668,0.475246434702793,339.897156860725));
#35509=CARTESIAN_POINT('Ctrl Pts',(95.774396124461,0.611373566642237,339.880103013719));
#35510=CARTESIAN_POINT('Ctrl Pts',(95.7666472394329,0.74753130285091,339.863045332646));
#35511=CARTESIAN_POINT('Ctrl Pts',(95.7588983544049,0.882938101519794,339.840289604601));
#35512=CARTESIAN_POINT('Ctrl Pts',(95.7511494693768,1.01708759408973,339.811934734434));
#35513=CARTESIAN_POINT('Ctrl Pts',(95.743392359602,1.15137947431728,339.783549768115));
#35514=CARTESIAN_POINT('Ctrl Pts',(95.7356352498273,1.28441099959263,339.74955386896));
#35515=CARTESIAN_POINT('Ctrl Pts',(95.7278781400526,1.41568794889479,339.710096675638));
#35516=CARTESIAN_POINT('Ctrl Pts',(95.7201168851264,1.54703504840114,339.670618397654));
#35517=CARTESIAN_POINT('Ctrl Pts',(95.7123556302003,1.67662533459653,339.625673138461));
#35518=CARTESIAN_POINT('Ctrl Pts',(95.7045943752741,1.8039831222545,339.575459316519));
#35519=CARTESIAN_POINT('Ctrl Pts',(95.6968207048694,1.93154464086691,339.525165168827));
#35520=CARTESIAN_POINT('Ctrl Pts',(95.6890470344647,2.0568661669874,339.469585775327));
#35521=CARTESIAN_POINT('Ctrl Pts',(95.6812733640601,2.17949443822818,339.408966665357));
#35522=CARTESIAN_POINT('Ctrl Pts',(95.673861559883,2.29641433393921,339.351169389542));
#35523=CARTESIAN_POINT('Ctrl Pts',(95.666449755706,2.41088582129536,339.288791173568));
#35524=CARTESIAN_POINT('Ctrl Pts',(95.659037951529,2.52254105490457,339.222081203485));
#35525=CARTESIAN_POINT('Ctrl Pts',(95.6512628727505,2.63966884411758,339.152101579049));
#35526=CARTESIAN_POINT('Ctrl Pts',(95.6434877939721,2.75406747873376,339.077133690981));
#35527=CARTESIAN_POINT('Ctrl Pts',(95.6357127151937,2.86528294307118,338.997416255364));
#35528=CARTESIAN_POINT('Ctrl Pts',(95.6279472041447,2.97636154969935,338.917796917126));
#35529=CARTESIAN_POINT('Ctrl Pts',(95.6201816930957,3.08426446528733,338.833439885998));
#35530=CARTESIAN_POINT('Ctrl Pts',(95.6124161820467,3.18856326497391,338.744629136211));
#35531=CARTESIAN_POINT('Ctrl Pts',(95.6046583705245,3.29275865209695,338.655906442541));
#35532=CARTESIAN_POINT('Ctrl Pts',(95.5969005590022,3.39335673908397,338.562739069829));
#35533=CARTESIAN_POINT('Ctrl Pts',(95.58914274748,3.48995934150991,338.465453340778));
#35534=CARTESIAN_POINT('Ctrl Pts',(95.581390773957,3.58648924741407,338.368240822323));
#35535=CARTESIAN_POINT('Ctrl Pts',(95.573638800434,3.6790293791985,338.266916392567));
#35536=CARTESIAN_POINT('Ctrl Pts',(95.565886826911,3.76721610358526,338.161845330086));
#35537=CARTESIAN_POINT('Ctrl Pts',(95.5581381363534,3.85536548084189,338.056818765263));
#35538=CARTESIAN_POINT('Ctrl Pts',(95.5503894457958,3.93916486686945,337.948049022325));
#35539=CARTESIAN_POINT('Ctrl Pts',(95.5426407552382,4.01828901506963,337.835936609635));
#35540=CARTESIAN_POINT('Ctrl Pts',(95.5348936768603,4.09739670082993,337.72384752287));
#35541=CARTESIAN_POINT('Ctrl Pts',(95.5271465984825,4.1718308583338,337.608417468844));
#35542=CARTESIAN_POINT('Ctrl Pts',(95.5193995201046,4.24130816114614,337.490077939482));
#35543=CARTESIAN_POINT('Ctrl Pts',(95.5116523767988,4.31078604624514,337.371737418321));
#35544=CARTESIAN_POINT('Ctrl Pts',(95.503905233493,4.37530679589446,337.250487710264));
#35545=CARTESIAN_POINT('Ctrl Pts',(95.4961580901872,4.43463205418474,337.126786685706));
#35546=CARTESIAN_POINT('Ctrl Pts',(95.4884092051591,4.4939706500526,337.003057850532));
#35547=CARTESIAN_POINT('Ctrl Pts',(95.480660320131,4.54811126126718,336.876876954585));
#35548=CARTESIAN_POINT('Ctrl Pts',(95.4729114351029,4.5968630339452,336.74872333708));
#35549=CARTESIAN_POINT('Ctrl Pts',(95.4651543253282,4.64566655225844,336.620433696001));
#35550=CARTESIAN_POINT('Ctrl Pts',(95.4573972155535,4.68906966706212,336.490167516577));
#35551=CARTESIAN_POINT('Ctrl Pts',(95.4496401057787,4.72693076135279,336.358421377878));
#35552=CARTESIAN_POINT('Ctrl Pts',(95.4418788508526,4.76481208740169,336.226604838256));
#35553=CARTESIAN_POINT('Ctrl Pts',(95.4341175959264,4.79714539983116,336.093307143199));
#35554=CARTESIAN_POINT('Ctrl Pts',(95.4263563410002,4.82384013238535,335.959035682177));
#35555=CARTESIAN_POINT('Ctrl Pts',(95.4185826705956,4.85057756781183,335.824549430576));
#35556=CARTESIAN_POINT('Ctrl Pts',(95.4108090001909,4.87165833881507,335.689086686676));
#35557=CARTESIAN_POINT('Ctrl Pts',(95.4030353297863,4.88704362996701,335.553161478502));
#35558=CARTESIAN_POINT('Ctrl Pts',(95.3956235256092,4.90171273211439,335.42356362147));
#35559=CARTESIAN_POINT('Ctrl Pts',(95.388211721432,4.91120464970279,335.293545673685));
#35560=CARTESIAN_POINT('Ctrl Pts',(95.3807999172549,4.91552986634681,335.163551813052));
#35561=CARTESIAN_POINT('Ctrl Pts',(95.3730248384765,4.92006707474269,335.027186566078));
#35562=CARTESIAN_POINT('Ctrl Pts',(95.3652497596981,4.91893264367984,334.890416887752));
#35563=CARTESIAN_POINT('Ctrl Pts',(95.3574746809196,4.91208162066749,334.753753752515));
#35564=CARTESIAN_POINT('Ctrl Pts',(95.3497091698706,4.9052390282751,334.617258789966));
#35565=CARTESIAN_POINT('Ctrl Pts',(95.3419436588216,4.89269386021368,334.480870496291));
#35566=CARTESIAN_POINT('Ctrl Pts',(95.3341781477726,4.8744530711977,334.345102817847));
#35567=CARTESIAN_POINT('Ctrl Pts',(95.3264203362504,4.85623036797715,334.209469753453));
#35568=CARTESIAN_POINT('Ctrl Pts',(95.3186625247282,4.83232333381084,334.074456464622));
#35569=CARTESIAN_POINT('Ctrl Pts',(95.310904713206,4.80279089998048,333.940574385072));
#35570=CARTESIAN_POINT('Ctrl Pts',(95.303152739683,4.7732806902431,333.806793056033));
#35571=CARTESIAN_POINT('Ctrl Pts',(95.29540076616,4.73815359085979,333.674141622023));
#35572=CARTESIAN_POINT('Ctrl Pts',(95.287648792637,4.69751998954568,333.54312354322));
#35573=CARTESIAN_POINT('Ctrl Pts',(95.2799001020794,4.65690359658586,333.412160950652));
#35574=CARTESIAN_POINT('Ctrl Pts',(95.2721514115218,4.61078545543573,333.282830710049));
#35575=CARTESIAN_POINT('Ctrl Pts',(95.2644027209641,4.55932635252582,333.155623066273));
#35576=CARTESIAN_POINT('Ctrl Pts',(95.2566556425863,4.50787795611206,333.02844188911));
#35577=CARTESIAN_POINT('Ctrl Pts',(95.2489085642085,4.45109095474543,332.903382792473));
#35578=CARTESIAN_POINT('Ctrl Pts',(95.2411614858307,4.38917487500052,332.780917536646));
#35579=CARTESIAN_POINT('Ctrl Pts',(95.2334143425249,4.32725827633928,332.658451254443));
#35580=CARTESIAN_POINT('Ctrl Pts',(95.2256671992191,4.26021268991968,332.538579205236));
#35581=CARTESIAN_POINT('Ctrl Pts',(95.2179200559133,4.18829416066721,332.42174960754));
#35582=CARTESIAN_POINT('Ctrl Pts',(95.2101711708852,4.11635946260249,332.304893744069));
#35583=CARTESIAN_POINT('Ctrl Pts',(95.2024222858571,4.0395498465652,332.191082026005));
#35584=CARTESIAN_POINT('Ctrl Pts',(95.194673400829,3.95816511713959,332.080734344401));
#35585=CARTESIAN_POINT('Ctrl Pts',(95.1869162910543,3.87669400512125,331.970269538628));
#35586=CARTESIAN_POINT('Ctrl Pts',(95.1791591812796,3.7906383116269,331.863276429067));
#35587=CARTESIAN_POINT('Ctrl Pts',(95.1714020715048,3.7003389835044,331.760142831905));
#35588=CARTESIAN_POINT('Ctrl Pts',(95.1636408165787,3.60999140230822,331.656954123446));
#35589=CARTESIAN_POINT('Ctrl Pts',(95.1558795616525,3.51539593739415,331.557629319808));
#35590=CARTESIAN_POINT('Ctrl Pts',(95.1481183067264,3.41693025279318,331.462519157642));
#35591=CARTESIAN_POINT('Ctrl Pts',(95.1403446363217,3.31830705518674,331.367256850213));
#35592=CARTESIAN_POINT('Ctrl Pts',(95.1325709659171,3.21580155867471,331.276222916564));
#35593=CARTESIAN_POINT('Ctrl Pts',(95.1247972955124,3.10982501513417,331.189728167473));
#35594=CARTESIAN_POINT('Ctrl Pts',(95.1173854913353,3.00878170519172,331.107259769763));
#35595=CARTESIAN_POINT('Ctrl Pts',(95.1099736871582,2.90458346034091,331.028917641786));
#35596=CARTESIAN_POINT('Ctrl Pts',(95.1025618829811,2.79760947254461,330.954933337802));
#35597=CARTESIAN_POINT('Ctrl Pts',(95.0947868042026,2.68539237094752,330.877322842691));
#35598=CARTESIAN_POINT('Ctrl Pts',(95.0870117254242,2.56976592484781,330.804262889189));
#35599=CARTESIAN_POINT('Ctrl Pts',(95.0792366466458,2.45113549718315,330.736067796394));
#35600=CARTESIAN_POINT('Ctrl Pts',(95.0714711355968,2.33265105181212,330.667956622003));
#35601=CARTESIAN_POINT('Ctrl Pts',(95.0637056245478,2.21117031566477,330.604698589799));
#35602=CARTESIAN_POINT('Ctrl Pts',(95.0559401134988,2.08712924079251,330.546565977279));
#35603=CARTESIAN_POINT('Ctrl Pts',(95.0481823019766,1.96321115300712,330.488491003414));
#35604=CARTESIAN_POINT('Ctrl Pts',(95.0404244904544,1.83673813007454,330.435531500831));
#35605=CARTESIAN_POINT('Ctrl Pts',(95.0326666789322,1.70817213861591,330.38791467909));
#35606=CARTESIAN_POINT('Ctrl Pts',(95.0249147054091,1.579702897143,330.340333690516));
#35607=CARTESIAN_POINT('Ctrl Pts',(95.0171627318861,1.44914418722087,330.298087515311));
#35608=CARTESIAN_POINT('Ctrl Pts',(95.0094107583631,1.31697911638087,330.26135577728));
#35609=CARTESIAN_POINT('Ctrl Pts',(95.0016620678055,1.18487001752685,330.224639595162));
#35610=CARTESIAN_POINT('Ctrl Pts',(94.9939133772479,1.05115628662986,330.193433309785));
#35611=CARTESIAN_POINT('Ctrl Pts',(94.9861646866903,0.916337191815168,330.167867012033));
#35612=CARTESIAN_POINT('Ctrl Pts',(94.9784176083124,0.78154614723918,330.142306033563));
#35613=CARTESIAN_POINT('Ctrl Pts',(94.9706705299346,0.645650579981453,330.122382781431));
#35614=CARTESIAN_POINT('Ctrl Pts',(94.9629234515567,0.509160590181383,330.108176356827));
#35615=CARTESIAN_POINT('Ctrl Pts',(94.9551763082509,0.372669456463735,330.09396981316));
#35616=CARTESIAN_POINT('Ctrl Pts',(94.9474291649451,0.235584279041177,330.085480233053));
#35617=CARTESIAN_POINT('Ctrl Pts',(94.9396820216393,0.0984205350251209,
330.082734859621));
#35618=CARTESIAN_POINT('Ctrl Pts',(94.9319331366112,-0.0387740463125655,
330.079988868971));
#35619=CARTESIAN_POINT('Ctrl Pts',(94.9241842515831,-0.176046838672367,
330.082989662599));
#35620=CARTESIAN_POINT('Ctrl Pts',(94.916435366555,-0.312882505244331,330.091712355575));
#35621=CARTESIAN_POINT('Ctrl Pts',(94.9086782567803,-0.449863410606665,
330.100444306909));
#35622=CARTESIAN_POINT('Ctrl Pts',(94.9009211470056,-0.586405872659239,
330.114910264639));
#35623=CARTESIAN_POINT('Ctrl Pts',(94.8931640372308,-0.721999262592784,
330.13503338888));
#35624=CARTESIAN_POINT('Ctrl Pts',(94.8854027823047,-0.857665109298382,
330.155167266275));
#35625=CARTESIAN_POINT('Ctrl Pts',(94.8776415273785,-0.99238048963109,330.180964260322));
#35626=CARTESIAN_POINT('Ctrl Pts',(94.8698802724523,-1.12564608597999,330.212296589009));
#35627=CARTESIAN_POINT('Ctrl Pts',(94.8621066020477,-1.25912486385199,330.24367903921));
#35628=CARTESIAN_POINT('Ctrl Pts',(94.854332931643,-1.39114884670889,330.280614413062));
#35629=CARTESIAN_POINT('Ctrl Pts',(94.8465592612384,-1.52123411514601,330.322925077635));
#35630=CARTESIAN_POINT('Ctrl Pts',(94.8391474570613,-1.64526388304059,330.363266170593));
#35631=CARTESIAN_POINT('Ctrl Pts',(94.8317356528842,-1.76753109899429,330.408493276942));
#35632=CARTESIAN_POINT('Ctrl Pts',(94.8243238487071,-1.88763584156343,330.458412833365));
#35633=CARTESIAN_POINT('Ctrl Pts',(94.8165487699287,-2.01362727533945,330.510779095951));
#35634=CARTESIAN_POINT('Ctrl Pts',(94.8087736911502,-2.13763705353376,330.568474908239));
#35635=CARTESIAN_POINT('Ctrl Pts',(94.8009986123718,-2.25918149336502,330.631329487986));
#35636=CARTESIAN_POINT('Ctrl Pts',(94.7932331013228,-2.38057636502517,330.694106721172));
#35637=CARTESIAN_POINT('Ctrl Pts',(94.7854675902738,-2.49951159074864,330.762029912906));
#35638=CARTESIAN_POINT('Ctrl Pts',(94.7777020792248,-2.6155222879101,330.834879806783));
#35639=CARTESIAN_POINT('Ctrl Pts',(94.7699442677026,-2.73141796012757,330.907657469778));
#35640=CARTESIAN_POINT('Ctrl Pts',(94.7621864561804,-2.84439454541985,330.985351907283));
#35641=CARTESIAN_POINT('Ctrl Pts',(94.7544286446582,-2.954010981776,331.067697597838));
#35642=CARTESIAN_POINT('Ctrl Pts',(94.7466766711352,-3.0635449282875,331.14998132065));
#35643=CARTESIAN_POINT('Ctrl Pts',(94.7389246976122,-3.16972344769618,331.236909095683));
#35644=CARTESIAN_POINT('Ctrl Pts',(94.7311727240892,-3.27213405330532,331.328171872255));
#35645=CARTESIAN_POINT('Ctrl Pts',(94.7234240335316,-3.37450128796226,331.419395998987));
#35646=CARTESIAN_POINT('Ctrl Pts',(94.715675342974,-3.47310349137332,331.514951216322));
#35647=CARTESIAN_POINT('Ctrl Pts',(94.7079266524164,-3.56756108470789,331.614488078683));
#35648=CARTESIAN_POINT('Ctrl Pts',(94.7001795740386,-3.66199902535125,331.714004231569));
#35649=CARTESIAN_POINT('Ctrl Pts',(94.6924324956608,-3.75229380224291,331.817500098356));
#35650=CARTESIAN_POINT('Ctrl Pts',(94.684685417283,-3.83810285304755,331.924589531147));
#35651=CARTESIAN_POINT('Ctrl Pts',(94.6769382739772,-3.92391262301458,332.031679861451));
#35652=CARTESIAN_POINT('Ctrl Pts',(94.6691911306714,-4.00523634749315,332.142363512802));
#35653=CARTESIAN_POINT('Ctrl Pts',(94.6614439873656,-4.08177216292266,332.256221752311));
#35654=CARTESIAN_POINT('Ctrl Pts',(94.6536951023375,-4.15832518522842,332.370105589571));
#35655=CARTESIAN_POINT('Ctrl Pts',(94.6459462173094,-4.23008793850525,332.48716511087));
#35656=CARTESIAN_POINT('Ctrl Pts',(94.6381973322813,-4.29680247070164,332.606953491828));
#35657=CARTESIAN_POINT('Ctrl Pts',(94.6304402225066,-4.36358781439183,332.726869017413));
#35658=CARTESIAN_POINT('Ctrl Pts',(94.6226831127319,-4.42531404294046,332.849518846542));
#35659=CARTESIAN_POINT('Ctrl Pts',(94.6149260029572,-4.48176944209824,332.974431998087));
#35660=CARTESIAN_POINT('Ctrl Pts',(94.607164748031,-4.53825500921624,333.099411899226));
#35661=CARTESIAN_POINT('Ctrl Pts',(94.5994034931048,-4.5894639888321,333.226657170284));
#35662=CARTESIAN_POINT('Ctrl Pts',(94.5916422381787,-4.63523362615662,333.355678774252));
#35663=CARTESIAN_POINT('Ctrl Pts',(94.583868567774,-4.68107647998455,333.484906770737));
#35664=CARTESIAN_POINT('Ctrl Pts',(94.5760948973694,-4.72146248878933,333.615916404672));
#35665=CARTESIAN_POINT('Ctrl Pts',(94.5683212269647,-4.7562791513337,333.748204610534));
#35666=CARTESIAN_POINT('Ctrl Pts',(94.5609094227876,-4.78947508986059,333.874334768588));
#35667=CARTESIAN_POINT('Ctrl Pts',(94.5534976186104,-4.8176084574982,334.001626861317));
#35668=CARTESIAN_POINT('Ctrl Pts',(94.5460858144332,-4.84062560532807,334.129639838031));
#35669=CARTESIAN_POINT('Ctrl Pts',(94.5342147471232,-4.87749086844671,334.334670978468));
#35670=CARTESIAN_POINT('Ctrl Pts',(94.5223436798131,-4.90133740109321,334.54210843251));
#35671=CARTESIAN_POINT('Ctrl Pts',(94.510472612503,-4.91192361891552,334.750621924701));
#35672=CARTESIAN_POINT('Ctrl Pts',(94.505827157832,-4.91606627885895,334.832218629611));
#35673=CARTESIAN_POINT('Ctrl Pts',(94.5011817031609,-4.91817873928009,334.913979820873));
#35674=CARTESIAN_POINT('Ctrl Pts',(94.4965362484899,-4.91824822735267,334.995824279422));
#35675=CARTESIAN_POINT('',(97.9965362484409,-4.91824934462186,335.002539020807));
#35676=CARTESIAN_POINT('Ctrl Pts',(97.9965362484409,-4.91824934462186,335.002539020807));
#35677=CARTESIAN_POINT('Ctrl Pts',(97.9879926354055,-4.91817110136582,335.154101324522));
#35678=CARTESIAN_POINT('Ctrl Pts',(97.9794490223701,-4.9110828885401,335.305421301889));
#35679=CARTESIAN_POINT('Ctrl Pts',(97.9709054093347,-4.89707624575504,335.455880802142));
#35680=CARTESIAN_POINT('Ctrl Pts',(97.9623163776358,-4.882995142318,335.607140159482));
#35681=CARTESIAN_POINT('Ctrl Pts',(97.9537273459368,-4.86192194224941,335.757529630768));
#35682=CARTESIAN_POINT('Ctrl Pts',(97.9451383142378,-4.83399989550252,335.906437020858));
#35683=CARTESIAN_POINT('Ctrl Pts',(97.9365257974073,-4.80600150104108,336.055751570889));
#35684=CARTESIAN_POINT('Ctrl Pts',(97.9279132805768,-4.77111687327354,336.203575703206));
#35685=CARTESIAN_POINT('Ctrl Pts',(97.9193007637463,-4.72953924477512,336.349311526161));
#35686=CARTESIAN_POINT('Ctrl Pts',(97.9106573473402,-4.68781244605122,336.495570213127));
#35687=CARTESIAN_POINT('Ctrl Pts',(97.902013930934,-4.63934465573974,336.639725363794));
#35688=CARTESIAN_POINT('Ctrl Pts',(97.8933705145278,-4.58437848914165,336.781195365701));
#35689=CARTESIAN_POINT('Ctrl Pts',(97.8905610849254,-4.5665124546577,336.827178341938));
#35690=CARTESIAN_POINT('Ctrl Pts',(97.887751655323,-4.54796023666128,336.872877826948));
#35691=CARTESIAN_POINT('Ctrl Pts',(97.8849422257206,-4.52873120316474,336.918274420406));
#35692=CARTESIAN_POINT('Ctrl Pts',(97.8771671469422,-4.47551497374203,337.043909207659));
#35693=CARTESIAN_POINT('Ctrl Pts',(97.8693920681638,-4.41698270373259,337.167526379649));
#35694=CARTESIAN_POINT('Ctrl Pts',(97.8616169893853,-4.35330843910294,337.288643418389));
#35695=CARTESIAN_POINT('Ctrl Pts',(97.8538514783363,-4.28971252970961,337.409611414902));
#35696=CARTESIAN_POINT('Ctrl Pts',(97.8460859672873,-4.22098739585917,337.528085056993));
#35697=CARTESIAN_POINT('Ctrl Pts',(97.8383204562383,-4.1473554295654,337.64360095388));
#35698=CARTESIAN_POINT('Ctrl Pts',(97.8305626447161,-4.07379646958064,337.759002316418));
#35699=CARTESIAN_POINT('Ctrl Pts',(97.8228048331939,-3.99534056779839,337.871451442333));
#35700=CARTESIAN_POINT('Ctrl Pts',(97.8150470216717,-3.91225621930559,337.980509073465));
#35701=CARTESIAN_POINT('Ctrl Pts',(97.8072950481487,-3.8292343944195,338.089484635271));
#35702=CARTESIAN_POINT('Ctrl Pts',(97.7995430746256,-3.74159129158938,338.195073472666));
#35703=CARTESIAN_POINT('Ctrl Pts',(97.7917911011026,-3.64963874108538,338.296865196223));
#35704=CARTESIAN_POINT('Ctrl Pts',(97.784042410545,-3.55772513254136,338.398613810925));
#35705=CARTESIAN_POINT('Ctrl Pts',(97.7762937199874,-3.46150596769722,338.496568220699));
#35706=CARTESIAN_POINT('Ctrl Pts',(97.7685450294297,-3.36133324847963,338.59035121613));
#35707=CARTESIAN_POINT('Ctrl Pts',(97.7607979510519,-3.26118137103292,338.684114699225));
#35708=CARTESIAN_POINT('Ctrl Pts',(97.7530508726741,-3.15707786052404,338.773708227315));
#35709=CARTESIAN_POINT('Ctrl Pts',(97.7453037942962,-3.04941117028915,338.858791854586));
#35710=CARTESIAN_POINT('Ctrl Pts',(97.7375566509904,-2.94174357770384,338.943876194939));
#35711=CARTESIAN_POINT('Ctrl Pts',(97.7298095076846,-2.83051305250342,339.024450316733));
#35712=CARTESIAN_POINT('Ctrl Pts',(97.7220623643788,-2.71614035732249,339.100215192136));
#35713=CARTESIAN_POINT('Ctrl Pts',(97.7143134793507,-2.60174194873155,339.175997101091));
#35714=CARTESIAN_POINT('Ctrl Pts',(97.7065645943227,-2.48420029024814,339.246967396325));
#35715=CARTESIAN_POINT('Ctrl Pts',(97.6988157092946,-2.36396393870532,339.31287115029));
#35716=CARTESIAN_POINT('Ctrl Pts',(97.6910585995198,-2.24359996705653,339.378844855179));
#35717=CARTESIAN_POINT('Ctrl Pts',(97.6833014897451,-2.12053593218395,339.43974108821));
#35718=CARTESIAN_POINT('Ctrl Pts',(97.6755443799704,-1.99524423475104,339.495351321776));
#35719=CARTESIAN_POINT('Ctrl Pts',(97.6677831250442,-1.86988558544098,339.550991271673));
#35720=CARTESIAN_POINT('Ctrl Pts',(97.660021870118,-1.74229726501254,339.601339450293));
#35721=CARTESIAN_POINT('Ctrl Pts',(97.6522606151919,-1.61296939884124,339.646236410354));
#35722=CARTESIAN_POINT('Ctrl Pts',(97.6444869447872,-1.483434650232,339.69120519092));
#35723=CARTESIAN_POINT('Ctrl Pts',(97.6367132743825,-1.35215516970395,339.730705214759));
#35724=CARTESIAN_POINT('Ctrl Pts',(97.6289396039779,-1.21963477132505,339.764627381766));
#35725=CARTESIAN_POINT('Ctrl Pts',(97.6215277998007,-1.09328322937226,339.796970463738));
#35726=CARTESIAN_POINT('Ctrl Pts',(97.6141159956236,-0.965803980530105,
339.824243240654));
#35727=CARTESIAN_POINT('Ctrl Pts',(97.6067041914464,-0.837638427861508,
339.846395044429));
#35728=CARTESIAN_POINT('Ctrl Pts',(97.598929112668,-0.703191099672106,339.869632574095));
#35729=CARTESIAN_POINT('Ctrl Pts',(97.5911540338895,-0.567563612605447,
339.887307884428));
#35730=CARTESIAN_POINT('Ctrl Pts',(97.5833789551111,-0.43125591259095,339.899306216226));
#35731=CARTESIAN_POINT('Ctrl Pts',(97.5756134440621,-0.295115947879001,
339.911289783313));
#35732=CARTESIAN_POINT('Ctrl Pts',(97.567847933013,-0.158297821345965,339.917610237824));
#35733=CARTESIAN_POINT('Ctrl Pts',(97.560082421964,-0.0213115572672648,
339.918203826604));
#35734=CARTESIAN_POINT('Ctrl Pts',(97.5523246104418,0.115538884531684,339.91879682684));
#35735=CARTESIAN_POINT('Ctrl Pts',(97.5445667989196,0.252556743763496,339.91367425961));
#35736=CARTESIAN_POINT('Ctrl Pts',(97.5368089873974,0.389227340773018,339.902824200366));
#35737=CARTESIAN_POINT('Ctrl Pts',(97.5290570138744,0.525795088824123,339.891982306136));
#35738=CARTESIAN_POINT('Ctrl Pts',(97.5213050403514,0.662015706729819,339.875421529783));
#35739=CARTESIAN_POINT('Ctrl Pts',(97.5135530668284,0.797375340014243,339.853182010768));
#35740=CARTESIAN_POINT('Ctrl Pts',(97.5058043762707,0.932677648413699,339.830951910201));
#35741=CARTESIAN_POINT('Ctrl Pts',(97.4980556857131,1.06711931250994,339.803047913489));
#35742=CARTESIAN_POINT('Ctrl Pts',(97.4903069951555,1.20019264041815,339.769561896903));
#35743=CARTESIAN_POINT('Ctrl Pts',(97.4825599167777,1.33323828130903,339.736082847361));
#35744=CARTESIAN_POINT('Ctrl Pts',(97.4748128383998,1.46491577346851,339.697024183348));
#35745=CARTESIAN_POINT('Ctrl Pts',(97.467065760022,1.59472903481945,339.652528599375));
#35746=CARTESIAN_POINT('Ctrl Pts',(97.4593186167162,1.72454338413047,339.608032642486));
#35747=CARTESIAN_POINT('Ctrl Pts',(97.4515714734104,1.85249310171334,339.558099801491));
#35748=CARTESIAN_POINT('Ctrl Pts',(97.4438243301046,1.97809902987863,339.502922083547));
#35749=CARTESIAN_POINT('Ctrl Pts',(97.4360754450765,2.10373319692309,339.44773196048));
#35750=CARTESIAN_POINT('Ctrl Pts',(97.4283265600483,2.22702216821446,339.387294771246));
#35751=CARTESIAN_POINT('Ctrl Pts',(97.4205776750202,2.34750882989827,339.32184976093));
#35752=CARTESIAN_POINT('Ctrl Pts',(97.4128205652455,2.46812337736981,339.256335286604));
#35753=CARTESIAN_POINT('Ctrl Pts',(97.4050634554708,2.58592932957166,339.185802560141));
#35754=CARTESIAN_POINT('Ctrl Pts',(97.3973063456961,2.70049568808664,339.110535987086));
#35755=CARTESIAN_POINT('Ctrl Pts',(97.3895450907699,2.81512326720042,339.03522919398));
#35756=CARTESIAN_POINT('Ctrl Pts',(97.3817838358437,2.92650748593328,338.955183741783));
#35757=CARTESIAN_POINT('Ctrl Pts',(97.3740225809175,3.03424902670012,338.870725501307));
#35758=CARTESIAN_POINT('Ctrl Pts',(97.3662489105129,3.14216291881931,338.786132155171));
#35759=CARTESIAN_POINT('Ctrl Pts',(97.3584752401082,3.24642219128993,338.69711216868));
#35760=CARTESIAN_POINT('Ctrl Pts',(97.3507015697036,3.34666245680582,338.604030169506));
#35761=CARTESIAN_POINT('Ctrl Pts',(97.3432897655266,3.44223651384464,338.515281159788));
#35762=CARTESIAN_POINT('Ctrl Pts',(97.3358779613495,3.53415711009659,338.422840004288));
#35763=CARTESIAN_POINT('Ctrl Pts',(97.3284661571725,3.6221427691649,338.327050468852));
#35764=CARTESIAN_POINT('Ctrl Pts',(97.3206910783941,3.71444086748068,338.226566002941));
#35765=CARTESIAN_POINT('Ctrl Pts',(97.3129159996156,3.80270022858172,338.122079080211));
#35766=CARTESIAN_POINT('Ctrl Pts',(97.3051409208372,3.88655379957592,338.013948013072));
#35767=CARTESIAN_POINT('Ctrl Pts',(97.2973754097882,3.97030418341263,337.905950008095));
#35768=CARTESIAN_POINT('Ctrl Pts',(97.2896098987392,4.04965932734085,337.79431708721));
#35769=CARTESIAN_POINT('Ctrl Pts',(97.2818443876902,4.12428961657313,337.679443640222));
#35770=CARTESIAN_POINT('Ctrl Pts',(97.274086576168,4.19884590965631,337.564684090591));
#35771=CARTESIAN_POINT('Ctrl Pts',(97.2663287646458,4.26868645930068,337.446690734555));
#35772=CARTESIAN_POINT('Ctrl Pts',(97.2585709531237,4.33352271520574,337.325889924157));
#35773=CARTESIAN_POINT('Ctrl Pts',(97.2508189796007,4.39831017977215,337.2051800202));
#35774=CARTESIAN_POINT('Ctrl Pts',(97.2430670060776,4.45810066231457,337.081667210123));
#35775=CARTESIAN_POINT('Ctrl Pts',(97.2353150325546,4.51264984081943,336.95580532688));
#35776=CARTESIAN_POINT('Ctrl Pts',(97.227566341997,4.56717591771481,336.82999674622));
#35777=CARTESIAN_POINT('Ctrl Pts',(97.2198176514394,4.61646495027763,336.701841428943));
#35778=CARTESIAN_POINT('Ctrl Pts',(97.2120689608818,4.66031945801409,336.571816023508));
#35779=CARTESIAN_POINT('Ctrl Pts',(97.204321882504,4.70416484145393,336.441817670944));
#35780=CARTESIAN_POINT('Ctrl Pts',(97.1965748041262,4.74257782426578,336.309950374288));
#35781=CARTESIAN_POINT('Ctrl Pts',(97.1888277257484,4.77540994283155,336.17670851973));
#35782=CARTESIAN_POINT('Ctrl Pts',(97.1810805824425,4.80824233656211,336.043465548477));
#35783=CARTESIAN_POINT('Ctrl Pts',(97.1733334391367,4.83549367923626,335.908848375866));
#35784=CARTESIAN_POINT('Ctrl Pts',(97.1655862958309,4.85706613404898,335.77336384191));
#35785=CARTESIAN_POINT('Ctrl Pts',(97.1578374108028,4.87864343880753,335.637848848155));
#35786=CARTESIAN_POINT('Ctrl Pts',(97.1500885257747,4.89453925369501,335.501466490962));
#35787=CARTESIAN_POINT('Ctrl Pts',(97.1423396407467,4.90470739447279,335.364730636366));
#35788=CARTESIAN_POINT('Ctrl Pts',(97.1345825309719,4.91488632782025,335.227849648921));
#35789=CARTESIAN_POINT('Ctrl Pts',(97.1268254211972,4.91932541382876,335.090614804979));
#35790=CARTESIAN_POINT('Ctrl Pts',(97.1190683114225,4.91803057721332,334.953542448463));
#35791=CARTESIAN_POINT('Ctrl Pts',(97.1113070564963,4.91673504867859,334.816396844861));
#35792=CARTESIAN_POINT('Ctrl Pts',(97.1035458015702,4.90969951221332,334.67941429186));
#35793=CARTESIAN_POINT('Ctrl Pts',(97.095784546644,4.89698190587674,334.54310693153));
#35794=CARTESIAN_POINT('Ctrl Pts',(97.0880108762394,4.88424395551469,334.406581523846));
#35795=CARTESIAN_POINT('Ctrl Pts',(97.0802372058347,4.86580582444609,334.270733854695));
#35796=CARTESIAN_POINT('Ctrl Pts',(97.0724635354301,4.84177694497911,334.136067666094));
#35797=CARTESIAN_POINT('Ctrl Pts',(97.0650517312529,4.8188666156321,334.007670220969));
#35798=CARTESIAN_POINT('Ctrl Pts',(97.0576399270758,4.79087438486096,333.880347017025));
#35799=CARTESIAN_POINT('Ctrl Pts',(97.0502281228986,4.75793700966978,333.754520785194));
#35800=CARTESIAN_POINT('Ctrl Pts',(97.0424530441202,4.72338527560537,333.622527434924));
#35801=CARTESIAN_POINT('Ctrl Pts',(97.0346779653417,4.68328219776451,333.491764385896));
#35802=CARTESIAN_POINT('Ctrl Pts',(97.0269028865633,4.6377304553138,333.362734204121));
#35803=CARTESIAN_POINT('Ctrl Pts',(97.0191373755143,4.59223476718217,333.233862802199));
#35804=CARTESIAN_POINT('Ctrl Pts',(97.0113718644653,4.54130388420285,333.106720389716));
#35805=CARTESIAN_POINT('Ctrl Pts',(97.0036063534162,4.48509108370171,332.981797573731));
#35806=CARTESIAN_POINT('Ctrl Pts',(96.995848541894,4.42893401835588,332.856998619081));
#35807=CARTESIAN_POINT('Ctrl Pts',(96.9880907303718,4.36750561684908,332.734415235493));
#35808=CARTESIAN_POINT('Ctrl Pts',(96.9803329188496,4.30100825658723,332.614520794627));
#35809=CARTESIAN_POINT('Ctrl Pts',(96.9725809453266,4.23456093769777,332.494716578129));
#35810=CARTESIAN_POINT('Ctrl Pts',(96.9648289718036,4.16305244155381,332.377597617088));
#35811=CARTESIAN_POINT('Ctrl Pts',(96.9570769982806,4.08673218930972,332.263614962152));
#35812=CARTESIAN_POINT('Ctrl Pts',(96.949328307723,4.01044425873778,332.149680578937));
#35813=CARTESIAN_POINT('Ctrl Pts',(96.9415796171654,3.92934884208925,332.038880184191));
#35814=CARTESIAN_POINT('Ctrl Pts',(96.9338309266078,3.84373989519572,331.931637785303));
#35815=CARTESIAN_POINT('Ctrl Pts',(96.9260838482299,3.75814875995866,331.824417699092));
#35816=CARTESIAN_POINT('Ctrl Pts',(96.9183367698521,3.66804620607121,331.720754441576));
#35817=CARTESIAN_POINT('Ctrl Pts',(96.9105896914743,3.57376763124534,331.621040399714));
#35818=CARTESIAN_POINT('Ctrl Pts',(96.9028425481685,3.47948826627414,331.521325522153));
#35819=CARTESIAN_POINT('Ctrl Pts',(96.8950954048626,3.38103307909655,331.425560210284));
#35820=CARTESIAN_POINT('Ctrl Pts',(96.8873482615568,3.27877533718385,331.33410101738));
#35821=CARTESIAN_POINT('Ctrl Pts',(96.8795993765287,3.17649460555992,331.242621262507));
#35822=CARTESIAN_POINT('Ctrl Pts',(96.8718504915006,3.07040990934296,331.155449813551));
#35823=CARTESIAN_POINT('Ctrl Pts',(96.8641016064725,2.96092837650429,331.072903590219));
#35824=CARTESIAN_POINT('Ctrl Pts',(96.8563444966978,2.85133063883543,330.990269751474));
#35825=CARTESIAN_POINT('Ctrl Pts',(96.8485873869231,2.73832917494129,330.912271180755));
#35826=CARTESIAN_POINT('Ctrl Pts',(96.8408302771484,2.62236139564555,330.839182319168));
#35827=CARTESIAN_POINT('Ctrl Pts',(96.8330690222222,2.50633164687649,330.76605440123));
#35828=CARTESIAN_POINT('Ctrl Pts',(96.825307767296,2.38733276318271,330.697841614454));
#35829=CARTESIAN_POINT('Ctrl Pts',(96.8175465123698,2.26582676936601,330.634772386951));
#35830=CARTESIAN_POINT('Ctrl Pts',(96.8097728419652,2.14412640555791,330.571602269239));
#35831=CARTESIAN_POINT('Ctrl Pts',(96.8019991715605,2.01991127168514,330.5135923183));
#35832=CARTESIAN_POINT('Ctrl Pts',(96.7942255011559,1.8936641952562,330.46092311388));
#35833=CARTESIAN_POINT('Ctrl Pts',(96.7868136969788,1.77329395060893,330.410705673599));
#35834=CARTESIAN_POINT('Ctrl Pts',(96.7794018928018,1.65107694982862,330.365343046185));
#35835=CARTESIAN_POINT('Ctrl Pts',(96.7719900886247,1.52744268343612,330.32494899372));
#35836=CARTESIAN_POINT('Ctrl Pts',(96.7642150098463,1.3977487333596,330.282575108416));
#35837=CARTESIAN_POINT('Ctrl Pts',(96.7564399310679,1.26608521919088,330.245535253123));
#35838=CARTESIAN_POINT('Ctrl Pts',(96.7486648522894,1.13293032499963,330.214015050045));
#35839=CARTESIAN_POINT('Ctrl Pts',(96.7408993412404,0.999939286382824,330.182533634583));
#35840=CARTESIAN_POINT('Ctrl Pts',(96.7331338301914,0.865460896067515,330.156558445819));
#35841=CARTESIAN_POINT('Ctrl Pts',(96.7253683191424,0.729990663153302,330.136226085208));
#35842=CARTESIAN_POINT('Ctrl Pts',(96.7176105076202,0.594654749369434,330.115913884193));
#35843=CARTESIAN_POINT('Ctrl Pts',(96.709852696098,0.458329334092584,330.101233434845));
#35844=CARTESIAN_POINT('Ctrl Pts',(96.7020948845758,0.321522003676771,330.092270722253));
#35845=CARTESIAN_POINT('Ctrl Pts',(96.6943429110528,0.184817625115412,330.083314754387));
#35846=CARTESIAN_POINT('Ctrl Pts',(96.6865909375298,0.0476324417326503,
330.080067984258));
#35847=CARTESIAN_POINT('Ctrl Pts',(96.6788389640067,-0.0895192722610985,
330.082564757682));
#35848=CARTESIAN_POINT('Ctrl Pts',(96.6710902734491,-0.22661290242245,330.08506047372));
#35849=CARTESIAN_POINT('Ctrl Pts',(96.6633415828915,-0.36367270139029,330.093294888352));
#35850=CARTESIAN_POINT('Ctrl Pts',(96.6555928923339,-0.500183035935528,
330.107250262576));
#35851=CARTESIAN_POINT('Ctrl Pts',(96.6478458139561,-0.636664968365415,
330.121202733268));
#35852=CARTESIAN_POINT('Ctrl Pts',(96.6400987355782,-0.77259727516104,330.140873756247));
#35853=CARTESIAN_POINT('Ctrl Pts',(96.6323516572004,-0.907468486810217,
330.166193631521));
#35854=CARTESIAN_POINT('Ctrl Pts',(96.6246045138946,-1.04234082880996,330.191513719));
#35855=CARTESIAN_POINT('Ctrl Pts',(96.6168573705888,-1.17615167376231,330.222482681083));
#35856=CARTESIAN_POINT('Ctrl Pts',(96.609110227283,-1.30839919196864,330.258979580622));
#35857=CARTESIAN_POINT('Ctrl Pts',(96.6013613422549,-1.44067644222476,330.29548468544));
#35858=CARTESIAN_POINT('Ctrl Pts',(96.5936124572268,-1.57138928963526,330.337520096779));
#35859=CARTESIAN_POINT('Ctrl Pts',(96.5858635721987,-1.70005090934896,330.384914955483));
#35860=CARTESIAN_POINT('Ctrl Pts',(96.578106462424,-1.82884909183523,330.43236011958));
#35861=CARTESIAN_POINT('Ctrl Pts',(96.5703493526493,-1.95559133011509,330.485175959176));
#35862=CARTESIAN_POINT('Ctrl Pts',(96.5625922428746,-2.07981013271289,330.543143162007));
#35863=CARTESIAN_POINT('Ctrl Pts',(96.5548309879484,-2.20409531386705,330.601141340658));
#35864=CARTESIAN_POINT('Ctrl Pts',(96.5470697330223,-2.32585402564403,330.664296187712));
#35865=CARTESIAN_POINT('Ctrl Pts',(96.5393084780961,-2.44464414984062,330.732342792216));
#35866=CARTESIAN_POINT('Ctrl Pts',(96.5315348076914,-2.56362429952231,330.800498249111));
#35867=CARTESIAN_POINT('Ctrl Pts',(96.5237611372868,-2.67962604125641,330.873560892135));
#35868=CARTESIAN_POINT('Ctrl Pts',(96.5159874668821,-2.79223623601205,330.951222423397));
#35869=CARTESIAN_POINT('Ctrl Pts',(96.508575662705,-2.89960439910991,331.025268791696));
#35870=CARTESIAN_POINT('Ctrl Pts',(96.5011638585279,-3.00388943220456,331.103495354437));
#35871=CARTESIAN_POINT('Ctrl Pts',(96.4937520543508,-3.10476324837013,331.18560250707));
#35872=CARTESIAN_POINT('Ctrl Pts',(96.4860800008919,-3.20917902781154,331.270592672663));
#35873=CARTESIAN_POINT('Ctrl Pts',(96.478407947433,-3.31028861217652,331.360025256184));
#35874=CARTESIAN_POINT('Ctrl Pts',(96.4707358939742,-3.40768282566073,331.453610170582));
#35875=CARTESIAN_POINT('Ctrl Pts',(96.4630733301437,-3.50495657141171,331.547079329002));
#35876=CARTESIAN_POINT('Ctrl Pts',(96.4554107663131,-3.59852379853239,331.644690328441));
#35877=CARTESIAN_POINT('Ctrl Pts',(96.4477482024826,-3.68800667994101,331.746111589005));
#35878=CARTESIAN_POINT('Ctrl Pts',(96.4400931667297,-3.77740164898974,331.84743320836));
#35879=CARTESIAN_POINT('Ctrl Pts',(96.4324381309767,-3.8627199896584,331.952557343243));
#35880=CARTESIAN_POINT('Ctrl Pts',(96.4247830952237,-3.94361955953311,332.06111452551));
#35881=CARTESIAN_POINT('Ctrl Pts',(96.4171337060828,-4.02445945516137,332.169591632344));
#35882=CARTESIAN_POINT('Ctrl Pts',(96.409484316942,-4.10088682606692,332.281496426618));
#35883=CARTESIAN_POINT('Ctrl Pts',(96.4018349278011,-4.17259913516054,332.396425626229));
#35884=CARTESIAN_POINT('Ctrl Pts',(96.394188539377,-4.24428331281478,332.511309741197));
#35885=CARTESIAN_POINT('Ctrl Pts',(96.3865421509528,-4.3112558936099,332.629215562045));
#35886=CARTESIAN_POINT('Ctrl Pts',(96.3788957625287,-4.37325731383819,332.749710345431));
#35887=CARTESIAN_POINT('Ctrl Pts',(96.3712506150443,-4.43524867179663,332.870185573603));
#35888=CARTESIAN_POINT('Ctrl Pts',(96.3636054675598,-4.49227028999564,332.993248571103));
#35889=CARTESIAN_POINT('Ctrl Pts',(96.3559603200754,-4.5441085445541,333.118441975965));
#35890=CARTESIAN_POINT('Ctrl Pts',(96.3483146550027,-4.59595030864192,333.243643856612));
#35891=CARTESIAN_POINT('Ctrl Pts',(96.3406689899301,-4.64260785844706,333.370976059466));
#35892=CARTESIAN_POINT('Ctrl Pts',(96.3330233248575,-4.68391591590268,333.499961748737));
#35893=CARTESIAN_POINT('Ctrl Pts',(96.3253714154608,-4.72525771023993,333.629052782465));
#35894=CARTESIAN_POINT('Ctrl Pts',(96.317719506064,-4.76124116337068,333.759799616223));
#35895=CARTESIAN_POINT('Ctrl Pts',(96.3100675966673,-4.79175099174716,333.891710554237));
#35896=CARTESIAN_POINT('Ctrl Pts',(96.3024124480701,-4.82227373552095,334.023677332688));
#35897=CARTESIAN_POINT('Ctrl Pts',(96.294757299473,-4.84731816497479,334.15680880187));
#35898=CARTESIAN_POINT('Ctrl Pts',(96.2871021508758,-4.86682048194327,334.29060486396));
#35899=CARTESIAN_POINT('Ctrl Pts',(96.279436680303,-4.88634909525836,334.424581332697));
#35900=CARTESIAN_POINT('Ctrl Pts',(96.2717712097301,-4.9003206283876,334.559223784412));
#35901=CARTESIAN_POINT('Ctrl Pts',(96.2641057391573,-4.90872329639167,334.694028331439));
#35902=CARTESIAN_POINT('Ctrl Pts',(96.2582492422806,-4.91514301954547,334.797020365799));
#35903=CARTESIAN_POINT('Ctrl Pts',(96.252392745404,-4.91831320390242,334.900106934656));
#35904=CARTESIAN_POINT('Ctrl Pts',(96.2465362485274,-4.91824904506439,335.003064836579));
#35905=CARTESIAN_POINT('',(99.7465362485345,-4.91824825774415,334.995860229884));
#35906=CARTESIAN_POINT('Ctrl Pts',(99.7465362484899,-4.91824825774482,334.995860230674));
#35907=CARTESIAN_POINT('Ctrl Pts',(99.738529339443,-4.91836754104053,335.137574614991));
#35908=CARTESIAN_POINT('Ctrl Pts',(99.7305224303961,-4.91235682468743,335.279387806484));
#35909=CARTESIAN_POINT('Ctrl Pts',(99.7225155213492,-4.90022160490974,335.420727091207));
#35910=CARTESIAN_POINT('Ctrl Pts',(99.7148038386915,-4.88853382834601,335.556854990807));
#35911=CARTESIAN_POINT('Ctrl Pts',(99.7070921560339,-4.87116521328685,335.692542885174));
#35912=CARTESIAN_POINT('Ctrl Pts',(99.6993804733762,-4.84817370561067,335.82728156194));
#35913=CARTESIAN_POINT('Ctrl Pts',(99.6916692052917,-4.82518343393723,335.962012995275));
#35914=CARTESIAN_POINT('Ctrl Pts',(99.6839579372071,-4.79657093696615,336.095794923497));
#35915=CARTESIAN_POINT('Ctrl Pts',(99.6762466691226,-4.76244560785376,336.22812657928));
#35916=CARTESIAN_POINT('Ctrl Pts',(99.6685341094029,-4.72831456275896,336.360480400576));
#35917=CARTESIAN_POINT('Ctrl Pts',(99.6608215496833,-4.68866894691457,336.49138308404));
#35918=CARTESIAN_POINT('Ctrl Pts',(99.6531089899637,-4.64366840174913,336.620347751903));
#35919=CARTESIAN_POINT('Ctrl Pts',(99.6453934318526,-4.59865036184059,336.749362557019));
#35920=CARTESIAN_POINT('Ctrl Pts',(99.6376778737415,-4.54827338055376,336.876437475271));
#35921=CARTESIAN_POINT('Ctrl Pts',(99.6299623156304,-4.49274555821127,337.001104797774));
#35922=CARTESIAN_POINT('Ctrl Pts',(99.6222378048506,-4.43715330473034,337.125916776724));
#35923=CARTESIAN_POINT('Ctrl Pts',(99.6145132940709,-4.37639844029515,337.248315222935));
#35924=CARTESIAN_POINT('Ctrl Pts',(99.6067887832912,-4.31073559827855,337.367855921342));
#35925=CARTESIAN_POINT('Ctrl Pts',(99.5990589508225,-4.24502751880551,337.487478975568));
#35926=CARTESIAN_POINT('Ctrl Pts',(99.5913291183538,-4.17440493187114,337.604240024921));
#35927=CARTESIAN_POINT('Ctrl Pts',(99.5835992858851,-4.09916563858818,337.717724071704));
#35928=CARTESIAN_POINT('Ctrl Pts',(99.5758583020993,-4.0238178025622,337.831371834402));
#35929=CARTESIAN_POINT('Ctrl Pts',(99.5681173183136,-3.9438401978577,337.94173284126));
#35930=CARTESIAN_POINT('Ctrl Pts',(99.5603763345278,-3.85957089418946,338.048425097526));
#35931=CARTESIAN_POINT('Ctrl Pts',(99.5583743668066,-3.83777722680782,338.076017772961));
#35932=CARTESIAN_POINT('Ctrl Pts',(99.5563723990853,-3.81569670409654,338.10336526122));
#35933=CARTESIAN_POINT('Ctrl Pts',(99.5543704313641,-3.79333556177948,338.130461368271));
#35934=CARTESIAN_POINT('Ctrl Pts',(99.5465953525857,-3.70649118299784,338.235695016484));
#35935=CARTESIAN_POINT('Ctrl Pts',(99.5388202738073,-3.61512721192145,338.337478397409));
#35936=CARTESIAN_POINT('Ctrl Pts',(99.5310451950288,-3.51954810874501,338.435398691961));
#35937=CARTESIAN_POINT('Ctrl Pts',(99.5232796839798,-3.42408662173995,338.533198489357));
#35938=CARTESIAN_POINT('Ctrl Pts',(99.5155141729308,-3.32442059367024,338.627144381986));
#35939=CARTESIAN_POINT('Ctrl Pts',(99.5077486618818,-3.22089536556936,338.716855674701));
#35940=CARTESIAN_POINT('Ctrl Pts',(99.4999908503596,-3.11747278303341,338.806478018407));
#35941=CARTESIAN_POINT('Ctrl Pts',(99.4922330388374,-3.01019890872618,338.891873863356));
#35942=CARTESIAN_POINT('Ctrl Pts',(99.4844752273152,-2.89945638686753,338.972698795926));
#35943=CARTESIAN_POINT('Ctrl Pts',(99.4767232537922,-2.78879720226804,339.053462905171));
#35944=CARTESIAN_POINT('Ctrl Pts',(99.4689712802691,-2.67467488018255,339.1296627192));
#35945=CARTESIAN_POINT('Ctrl Pts',(99.4612193067461,-2.55750536408549,339.200993855646));
#35946=CARTESIAN_POINT('Ctrl Pts',(99.4534706161884,-2.44038546934846,339.272294783313));
#35947=CARTESIAN_POINT('Ctrl Pts',(99.4457219256308,-2.32022128046657,339.338730931514));
#35948=CARTESIAN_POINT('Ctrl Pts',(99.4379732350732,-2.19745777822956,339.40004117883));
#35949=CARTESIAN_POINT('Ctrl Pts',(99.4302261566953,-2.07471981796444,339.461338670037));
#35950=CARTESIAN_POINT('Ctrl Pts',(99.4224790783175,-1.94938396952175,339.517512207143));
#35951=CARTESIAN_POINT('Ctrl Pts',(99.4147319999397,-1.82191952043152,339.568346782324));
#35952=CARTESIAN_POINT('Ctrl Pts',(99.4069848566339,-1.69445400306669,339.619181783548));
#35953=CARTESIAN_POINT('Ctrl Pts',(99.399237713328,-1.56486021253767,339.664677588801));
#35954=CARTESIAN_POINT('Ctrl Pts',(99.3914905700222,-1.43362673064403,339.704667624783));
#35955=CARTESIAN_POINT('Ctrl Pts',(99.3837416849941,-1.30236374467723,339.744666651374));
#35956=CARTESIAN_POINT('Ctrl Pts',(99.375992799966,-1.16946070762542,339.779157331668));
#35957=CARTESIAN_POINT('Ctrl Pts',(99.3682439149379,-1.03542026026359,339.808023288955));
#35958=CARTESIAN_POINT('Ctrl Pts',(99.3604868051631,-0.901237540986117,
339.836919884867));
#35959=CARTESIAN_POINT('Ctrl Pts',(99.3527296953884,-0.76591538250305,339.86017974944));
#35960=CARTESIAN_POINT('Ctrl Pts',(99.3449725856137,-0.629966042326224,
339.877737779752));
#35961=CARTESIAN_POINT('Ctrl Pts',(99.3372113306875,-0.49394405516901,339.895305192513));
#35962=CARTESIAN_POINT('Ctrl Pts',(99.3294500757614,-0.357294607722734,
339.907164666055));
#35963=CARTESIAN_POINT('Ctrl Pts',(99.3216888208352,-0.220532944755472,
339.913303194672));
#35964=CARTESIAN_POINT('Ctrl Pts',(99.3139151504305,-0.0835525076979857,
339.919451542934));
#35965=CARTESIAN_POINT('Ctrl Pts',(99.3061414800259,0.05354011251302,339.919860657402));
#35966=CARTESIAN_POINT('Ctrl Pts',(99.2983678096212,0.190230913560278,339.914569692458));
#35967=CARTESIAN_POINT('Ctrl Pts',(99.2909560054441,0.320558724932695,339.909525023205));
#35968=CARTESIAN_POINT('Ctrl Pts',(99.2835442012671,0.450520997721607,339.899299031945));
#35969=CARTESIAN_POINT('Ctrl Pts',(99.27613239709,0.579680216019076,339.883969073372));
#35970=CARTESIAN_POINT('Ctrl Pts',(99.2683573183115,0.715169912351052,339.867887747865));
#35971=CARTESIAN_POINT('Ctrl Pts',(99.2605822395331,0.850204016037191,339.846138663169));
#35972=CARTESIAN_POINT('Ctrl Pts',(99.2528071607547,0.984270617820415,339.818754446265));
#35973=CARTESIAN_POINT('Ctrl Pts',(99.2450416497056,1.11817224211523,339.791403927382));
#35974=CARTESIAN_POINT('Ctrl Pts',(99.2372761386566,1.25110835409944,339.758432151213));
#35975=CARTESIAN_POINT('Ctrl Pts',(99.2295106276076,1.38257193525139,339.719923506409));
#35976=CARTESIAN_POINT('Ctrl Pts',(99.2217528160854,1.51390516987935,339.681453043039));
#35977=CARTESIAN_POINT('Ctrl Pts',(99.2139950045632,1.64376840649856,339.637456745261));
#35978=CARTESIAN_POINT('Ctrl Pts',(99.206237193041,1.77166494960274,339.588070004789));
#35979=CARTESIAN_POINT('Ctrl Pts',(99.198485219518,1.89946524650248,339.538720429406));
#35980=CARTESIAN_POINT('Ctrl Pts',(99.1907332459951,2.02530143258804,339.483988625787));
#35981=CARTESIAN_POINT('Ctrl Pts',(99.1829812724721,2.14869245535333,339.42405965091));
#35982=CARTESIAN_POINT('Ctrl Pts',(99.1752325819145,2.27203122194747,339.364156055989));
#35983=CARTESIAN_POINT('Ctrl Pts',(99.1674838913568,2.39292653394667,339.299059837865));
#35984=CARTESIAN_POINT('Ctrl Pts',(99.1597352007992,2.51091800413993,339.229003882593));
#35985=CARTESIAN_POINT('Ctrl Pts',(99.1519881224214,2.62888492522242,339.158962503048));
#35986=CARTESIAN_POINT('Ctrl Pts',(99.1442410440435,2.74394887034699,339.083963638334));
#35987=CARTESIAN_POINT('Ctrl Pts',(99.1364939656657,2.85567507643598,339.004285569277));
#35988=CARTESIAN_POINT('Ctrl Pts',(99.1287468223599,2.96740221889789,338.924606832441));
#35989=CARTESIAN_POINT('Ctrl Pts',(99.1209996790541,3.07579124829143,338.840249039995));
#35990=CARTESIAN_POINT('Ctrl Pts',(99.1132525357483,3.18043768992683,338.751532908425));
#35991=CARTESIAN_POINT('Ctrl Pts',(99.1055036507201,3.28510765830452,338.662796831584));
#35992=CARTESIAN_POINT('Ctrl Pts',(99.097754765692,3.38603306651375,338.569700718547));
#35993=CARTESIAN_POINT('Ctrl Pts',(99.0900058806639,3.48284404313138,338.472604272549));
#35994=CARTESIAN_POINT('Ctrl Pts',(99.0822487708892,3.57975777591951,338.37540476738));
#35995=CARTESIAN_POINT('Ctrl Pts',(99.0744916611144,3.67254807700514,338.274196724711));
#35996=CARTESIAN_POINT('Ctrl Pts',(99.0667345513397,3.76088298801926,338.169375681886));
#35997=CARTESIAN_POINT('Ctrl Pts',(99.0589732964135,3.84926510238537,338.064498626046));
#35998=CARTESIAN_POINT('Ctrl Pts',(99.0512120414874,3.93318684365483,337.956005032031));
#35999=CARTESIAN_POINT('Ctrl Pts',(99.0434507865612,4.01235844654264,337.844321142023));
#36000=CARTESIAN_POINT('Ctrl Pts',(99.0356771161565,4.09165669819311,337.732458594188));
#36001=CARTESIAN_POINT('Ctrl Pts',(99.0279034457519,4.16618941444608,337.617395880424));
#36002=CARTESIAN_POINT('Ctrl Pts',(99.0201297753472,4.23571136490989,337.499586424926));
#36003=CARTESIAN_POINT('Ctrl Pts',(99.0127179711702,4.30199705185293,337.387261027926));
#36004=CARTESIAN_POINT('Ctrl Pts',(99.0053061669932,4.36372784067942,337.272439109477));
#36005=CARTESIAN_POINT('Ctrl Pts',(98.9978943628162,4.4207320156403,337.155530447104));
#36006=CARTESIAN_POINT('Ctrl Pts',(98.9901192840378,4.48053013502324,337.032891742934));
#36007=CARTESIAN_POINT('Ctrl Pts',(98.9823442052593,4.53531556746633,336.907569006628));
#36008=CARTESIAN_POINT('Ctrl Pts',(98.9745691264809,4.58483872621954,336.78001036993));
#36009=CARTESIAN_POINT('Ctrl Pts',(98.9668036154319,4.63430094357308,336.652608702255));
#36010=CARTESIAN_POINT('Ctrl Pts',(98.9590381043829,4.67851363163728,336.522976969615));
#36011=CARTESIAN_POINT('Ctrl Pts',(98.9512725933339,4.71727337781604,336.391587202244));
#36012=CARTESIAN_POINT('Ctrl Pts',(98.9435147818117,4.75599469359367,336.260327708209));
#36013=CARTESIAN_POINT('Ctrl Pts',(98.9357569702895,4.78927371705804,336.12731402079));
#36014=CARTESIAN_POINT('Ctrl Pts',(98.9279991587673,4.81695551155129,335.99303709006));
#36015=CARTESIAN_POINT('Ctrl Pts',(98.9202471852443,4.84461647461643,335.858861206979));
#36016=CARTESIAN_POINT('Ctrl Pts',(98.9124952117212,4.86668851407112,335.723424354053));
#36017=CARTESIAN_POINT('Ctrl Pts',(98.9047432381982,4.88306692316215,335.587231203547));
#36018=CARTESIAN_POINT('Ctrl Pts',(98.8969945476405,4.89943839598715,335.451095730922));
#36019=CARTESIAN_POINT('Ctrl Pts',(98.889245857083,4.91012098769387,335.314204985027));
#36020=CARTESIAN_POINT('Ctrl Pts',(98.8814971665253,4.91506139519829,335.177072143296));
#36021=CARTESIAN_POINT('Ctrl Pts',(98.8737500881475,4.92000077480966,335.039967833199));
#36022=CARTESIAN_POINT('Ctrl Pts',(98.8660030097696,4.91920033251634,334.902621917832));
#36023=CARTESIAN_POINT('Ctrl Pts',(98.8582559313918,4.91265880535237,334.765550592464));
#36024=CARTESIAN_POINT('Ctrl Pts',(98.850508788086,4.9061172233641,334.628478118307));
#36025=CARTESIAN_POINT('Ctrl Pts',(98.8427616447802,4.89383447916726,334.49168062917));
#36026=CARTESIAN_POINT('Ctrl Pts',(98.8350145014744,4.87586138563468,334.355671814541));
#36027=CARTESIAN_POINT('Ctrl Pts',(98.8272656164463,4.85788425136914,334.219632422244));
#36028=CARTESIAN_POINT('Ctrl Pts',(98.8195167314183,4.83421427327873,334.084382444714));
#36029=CARTESIAN_POINT('Ctrl Pts',(98.8117678463902,4.80495377483786,333.950427570784));
#36030=CARTESIAN_POINT('Ctrl Pts',(98.8040107366155,4.77566221900155,333.816330515765));
#36031=CARTESIAN_POINT('Ctrl Pts',(98.7962536268407,4.74076837296629,333.683531692784));
#36032=CARTESIAN_POINT('Ctrl Pts',(98.788496517066,4.70042521080144,333.552524300666));
#36033=CARTESIAN_POINT('Ctrl Pts',(98.7807352621398,4.66006049054065,333.421446902387));
#36034=CARTESIAN_POINT('Ctrl Pts',(98.7729740072136,4.61424078235331,333.292163210679));
#36035=CARTESIAN_POINT('Ctrl Pts',(98.7652127522875,4.56316771376261,333.165147559455));
#36036=CARTESIAN_POINT('Ctrl Pts',(98.7574390818828,4.51201294490686,333.037928724583));
#36037=CARTESIAN_POINT('Ctrl Pts',(98.7496654114782,4.4555881835977,332.912985536685));
#36038=CARTESIAN_POINT('Ctrl Pts',(98.7418917410735,4.39414201567991,332.790769589079));
#36039=CARTESIAN_POINT('Ctrl Pts',(98.7344799368964,4.3355561816615,332.674242823238));
#36040=CARTESIAN_POINT('Ctrl Pts',(98.7270681327193,4.27240605276472,332.56019535739));
#36041=CARTESIAN_POINT('Ctrl Pts',(98.7196563285422,4.2049432944078,332.448993345106));
#36042=CARTESIAN_POINT('Ctrl Pts',(98.7118812497637,4.13417398530278,332.332340990946));
#36043=CARTESIAN_POINT('Ctrl Pts',(98.7041061709853,4.05843496378142,332.218451428376));
#36044=CARTESIAN_POINT('Ctrl Pts',(98.6963310922068,3.97796800767736,332.107777050019));
#36045=CARTESIAN_POINT('Ctrl Pts',(98.6885655811578,3.89760007128557,331.997238863531));
#36046=CARTESIAN_POINT('Ctrl Pts',(98.6808000701088,3.81251600417157,331.889908302103));
#36047=CARTESIAN_POINT('Ctrl Pts',(98.6730345590598,3.72300266840189,331.78621186237));
#36048=CARTESIAN_POINT('Ctrl Pts',(98.6652767475376,3.6335780853656,331.682618237959));
#36049=CARTESIAN_POINT('Ctrl Pts',(98.6575189360155,3.53973322703933,331.582651858565));
#36050=CARTESIAN_POINT('Ctrl Pts',(98.6497611244933,3.44179709869773,331.486708694985));
#36051=CARTESIAN_POINT('Ctrl Pts',(98.6420091509703,3.34393467039838,331.390837731677));
#36052=CARTESIAN_POINT('Ctrl Pts',(98.6342571774473,3.2419873783973,331.298984230331));
#36053=CARTESIAN_POINT('Ctrl Pts',(98.6265052039243,3.13632294953612,331.211509348208));
#36054=CARTESIAN_POINT('Ctrl Pts',(98.6187565133667,3.03070326962321,331.12407151175));
#36055=CARTESIAN_POINT('Ctrl Pts',(98.6110078228091,2.92136988430319,331.041008855088));
#36056=CARTESIAN_POINT('Ctrl Pts',(98.6032591322515,2.80872549007244,330.962643911677));
#36057=CARTESIAN_POINT('Ctrl Pts',(98.5955120538736,2.69610453244866,330.884295272748));
#36058=CARTESIAN_POINT('Ctrl Pts',(98.5877649754958,2.58017425681572,330.810642626037));
#36059=CARTESIAN_POINT('Ctrl Pts',(98.580017897118,2.46136805932454,330.741966376479));
#36060=CARTESIAN_POINT('Ctrl Pts',(98.5722707538122,2.34256086612308,330.673289551348));
#36061=CARTESIAN_POINT('Ctrl Pts',(98.5645236105064,2.22087804139224,330.609589402173));
#36062=CARTESIAN_POINT('Ctrl Pts',(98.5567764672006,2.09677905534404,330.551101186184));
#36063=CARTESIAN_POINT('Ctrl Pts',(98.5490275821725,1.97265216920925,330.492599820803));
#36064=CARTESIAN_POINT('Ctrl Pts',(98.5412786971444,1.84610839434497,330.439312886872));
#36065=CARTESIAN_POINT('Ctrl Pts',(98.5335298121163,1.71762834838097,330.391427995644));
#36066=CARTESIAN_POINT('Ctrl Pts',(98.5257727023416,1.58901193236857,330.343492278896));
#36067=CARTESIAN_POINT('Ctrl Pts',(98.5180155925669,1.45845550668665,330.300970195345));
#36068=CARTESIAN_POINT('Ctrl Pts',(98.5102584827922,1.32645659579741,330.264000004015));
#36069=CARTESIAN_POINT('Ctrl Pts',(98.502497227866,1.19438714891078,330.227010056998));
#36070=CARTESIAN_POINT('Ctrl Pts',(98.4947359729398,1.06087406117239,330.195578003253));
#36071=CARTESIAN_POINT('Ctrl Pts',(98.4869747180137,0.926425322311606,330.169790979194));
#36072=CARTESIAN_POINT('Ctrl Pts',(98.479201047609,0.791761509285206,330.143962704299));
#36073=CARTESIAN_POINT('Ctrl Pts',(98.4714273772044,0.656159441039006,330.123797561643));
#36074=CARTESIAN_POINT('Ctrl Pts',(98.4636537067997,0.520133396093588,330.109330893143));
#36075=CARTESIAN_POINT('Ctrl Pts',(98.4562419026226,0.390439396265707,330.095537651541));
#36076=CARTESIAN_POINT('Ctrl Pts',(98.4488300984455,0.260360290838765,330.086924314367));
#36077=CARTESIAN_POINT('Ctrl Pts',(98.4414182942683,0.130340176758547,330.083477397507));
#36078=CARTESIAN_POINT('Ctrl Pts',(98.4336432154899,-0.00605261042199617,
330.079861536984));
#36079=CARTESIAN_POINT('Ctrl Pts',(98.4258681367115,-0.142811503763694,
330.081919918714));
#36080=CARTESIAN_POINT('Ctrl Pts',(98.4180930579331,-0.279425236798542,
330.089694042166));
#36081=CARTESIAN_POINT('Ctrl Pts',(98.410327546884,-0.415870857937821,330.097458599064));
#36082=CARTESIAN_POINT('Ctrl Pts',(98.402562035835,-0.552171287678357,330.110924880874));
#36083=CARTESIAN_POINT('Ctrl Pts',(98.394796524786,-0.68781263837535,330.130082460966));
#36084=CARTESIAN_POINT('Ctrl Pts',(98.3870387132638,-0.823319500277665,
330.149221046262));
#36085=CARTESIAN_POINT('Ctrl Pts',(98.3792809017416,-0.958168199056252,
330.174039645761));
#36086=CARTESIAN_POINT('Ctrl Pts',(98.3715230902194,-1.09184771078839,330.204475874428));
#36087=CARTESIAN_POINT('Ctrl Pts',(98.3637711166964,-1.22542662444972,330.234889198868));
#36088=CARTESIAN_POINT('Ctrl Pts',(98.3560191431733,-1.3578377227775,330.27091165153));
#36089=CARTESIAN_POINT('Ctrl Pts',(98.3482671696503,-1.4885783028302,330.312429445988));
#36090=CARTESIAN_POINT('Ctrl Pts',(98.3405184790927,-1.6192635141691,330.353929657634));
#36091=CARTESIAN_POINT('Ctrl Pts',(98.332769788535,-1.74827924256604,330.400920464221));
#36092=CARTESIAN_POINT('Ctrl Pts',(98.3250210979774,-1.87513634057516,330.453237771034));
#36093=CARTESIAN_POINT('Ctrl Pts',(98.3172740195996,-2.00196704490534,330.505544192794));
#36094=CARTESIAN_POINT('Ctrl Pts',(98.3095269412218,-2.12663965105759,330.563174761514));
#36095=CARTESIAN_POINT('Ctrl Pts',(98.3017798628439,-2.24868382501489,330.625916768325));
#36096=CARTESIAN_POINT('Ctrl Pts',(98.2940327195381,-2.37072902181983,330.688659300975));
#36097=CARTESIAN_POINT('Ctrl Pts',(98.2862855762323,-2.4901453948647,330.756513178448));
#36098=CARTESIAN_POINT('Ctrl Pts',(98.2785384329265,-2.60648646563008,330.829219333627));
#36099=CARTESIAN_POINT('Ctrl Pts',(98.2707895478984,-2.722853692338,330.901941834694));
#36100=CARTESIAN_POINT('Ctrl Pts',(98.2630406628703,-2.8361439095662,330.979518577117));
#36101=CARTESIAN_POINT('Ctrl Pts',(98.2552917778422,-2.94593926123445,331.061646926491));
#36102=CARTESIAN_POINT('Ctrl Pts',(98.2475346680675,-3.05585115082365,331.143862447744));
#36103=CARTESIAN_POINT('Ctrl Pts',(98.2397775582927,-3.16226045131371,331.230638992073));
#36104=CARTESIAN_POINT('Ctrl Pts',(98.232020448518,-3.2647816587051,331.321633000436));
#36105=CARTESIAN_POINT('Ctrl Pts',(98.2242591935918,-3.36735765015165,331.412675633087));
#36106=CARTESIAN_POINT('Ctrl Pts',(98.2164979386657,-3.46604112747362,331.507939949091));
#36107=CARTESIAN_POINT('Ctrl Pts',(98.2087366837395,-3.56048391341217,331.60704592356));
#36108=CARTESIAN_POINT('Ctrl Pts',(98.2009630133348,-3.65507777702939,331.706310435289));
#36109=CARTESIAN_POINT('Ctrl Pts',(98.1931893429302,-3.7454171356662,331.809428591653));
#36110=CARTESIAN_POINT('Ctrl Pts',(98.1854156725255,-3.83119396393381,331.915987050413));
#36111=CARTESIAN_POINT('Ctrl Pts',(98.1780038683485,-3.91297786020839,332.017585187281));
#36112=CARTESIAN_POINT('Ctrl Pts',(98.1705920641714,-3.99061426707868,332.122310311172));
#36113=CARTESIAN_POINT('Ctrl Pts',(98.1631802599944,-4.06387419728365,332.229781674461));
#36114=CARTESIAN_POINT('Ctrl Pts',(98.1552885578527,-4.14187754630421,332.344211571363));
#36115=CARTESIAN_POINT('Ctrl Pts',(98.1473968557111,-4.21516087342881,332.462109660984));
#36116=CARTESIAN_POINT('Ctrl Pts',(98.1395051535695,-4.28340595589162,332.583056376427));
#36117=CARTESIAN_POINT('Ctrl Pts',(98.1316239051704,-4.35156063751223,332.703842879814));
#36118=CARTESIAN_POINT('Ctrl Pts',(98.1237426567713,-4.41469017547625,332.827669647362));
#36119=CARTESIAN_POINT('Ctrl Pts',(98.1158614083722,-4.47251859532413,332.954086884303));
#36120=CARTESIAN_POINT('Ctrl Pts',(98.1079890773332,-4.53028158431405,333.080361084511));
#36121=CARTESIAN_POINT('Ctrl Pts',(98.1001167462942,-4.58275524058733,333.209219580141));
#36122=CARTESIAN_POINT('Ctrl Pts',(98.0922444152552,-4.62970875904289,333.340186796973));
#36123=CARTESIAN_POINT('Ctrl Pts',(98.0842687346914,-4.67727869261043,333.472873377429));
#36124=CARTESIAN_POINT('Ctrl Pts',(98.0762930541276,-4.71918230838665,333.607724111206));
#36125=CARTESIAN_POINT('Ctrl Pts',(98.0683173735638,-4.75522891826669,333.744220959969));
#36126=CARTESIAN_POINT('Ctrl Pts',(98.0604592572084,-4.79074418901906,333.87870579937));
#36127=CARTESIAN_POINT('Ctrl Pts',(98.052601140853,-4.8205738361938,334.014788181689));
#36128=CARTESIAN_POINT('Ctrl Pts',(98.0447430244975,-4.84458495519773,334.151955381851));
#36129=CARTESIAN_POINT('Ctrl Pts',(98.0367085618296,-4.86913491482242,334.292200791707));
#36130=CARTESIAN_POINT('Ctrl Pts',(98.0286740991616,-4.88760196514298,334.433579907344));
#36131=CARTESIAN_POINT('Ctrl Pts',(98.0206396364937,-4.89989898113148,334.57553205397));
#36132=CARTESIAN_POINT('Ctrl Pts',(98.0126051738258,-4.91219599711999,334.717484200597));
#36133=CARTESIAN_POINT('Ctrl Pts',(98.0045707111579,-4.91832292500355,334.860008960813));
#36134=CARTESIAN_POINT('Ctrl Pts',(97.9965362484899,-4.91824934462231,335.002539019938));
#36135=CARTESIAN_POINT('',(101.496536248439,-4.91824996307027,334.999397290091));
#36136=CARTESIAN_POINT('Ctrl Pts',(101.496536248439,-4.91824996307028,334.999397290091));
#36137=CARTESIAN_POINT('Ctrl Pts',(101.488787543807,-4.91826662769589,335.135384425997));
#36138=CARTESIAN_POINT('Ctrl Pts',(101.481038839174,-4.91263905510794,335.271593521368));
#36139=CARTESIAN_POINT('Ctrl Pts',(101.473290134542,-4.90133800926562,335.407515375695));
#36140=CARTESIAN_POINT('Ctrl Pts',(101.465550940153,-4.89005083357312,335.543270408605));
#36141=CARTESIAN_POINT('Ctrl Pts',(101.457811745764,-4.87310406998696,335.678738513187));
#36142=CARTESIAN_POINT('Ctrl Pts',(101.450072551375,-4.85052045818359,335.813409089722));
#36143=CARTESIAN_POINT('Ctrl Pts',(101.442340971951,-4.82795906748272,335.947947157396));
#36144=CARTESIAN_POINT('Ctrl Pts',(101.434609392528,-4.79977192949126,336.081688872592));
#36145=CARTESIAN_POINT('Ctrl Pts',(101.426877813105,-4.76603365967239,336.214127759904));
#36146=CARTESIAN_POINT('Ctrl Pts',(101.419151960248,-4.73232037885692,336.346468553395));
#36147=CARTESIAN_POINT('Ctrl Pts',(101.411426107392,-4.6930642460017,336.47750805938));
#36148=CARTESIAN_POINT('Ctrl Pts',(101.403700254536,-4.64839105527419,336.606749407887));
#36149=CARTESIAN_POINT('Ctrl Pts',(101.395977514058,-4.6037358612468,336.735938691213));
#36150=CARTESIAN_POINT('Ctrl Pts',(101.388254773579,-4.5536680771719,336.863330886013));
#36151=CARTESIAN_POINT('Ctrl Pts',(101.380532033101,-4.49836344221849,336.98844396557));
#36152=CARTESIAN_POINT('Ctrl Pts',(101.37281075426,-4.44306927444177,337.113533365725));
#36153=CARTESIAN_POINT('Ctrl Pts',(101.365089475418,-4.38254038615454,337.236344148507));
#36154=CARTESIAN_POINT('Ctrl Pts',(101.357368196577,-4.31700061305907,337.356414388292));
#36155=CARTESIAN_POINT('Ctrl Pts',(101.349646678094,-4.25145880583766,337.476488354637));
#36156=CARTESIAN_POINT('Ctrl Pts',(101.341925159611,-4.18090599301653,337.593821263021));
#36157=CARTESIAN_POINT('Ctrl Pts',(101.334203641128,-4.10561169630126,337.707976303754));
#36158=CARTESIAN_POINT('Ctrl Pts',(101.326480181903,-4.03029847497236,337.822160036435));
#36159=CARTESIAN_POINT('Ctrl Pts',(101.318756722679,-3.95024161557251,337.933163983724));
#36160=CARTESIAN_POINT('Ctrl Pts',(101.311033263455,-3.86575338025264,338.040581172336));
#36161=CARTESIAN_POINT('Ctrl Pts',(101.303301555462,-3.78117491025085,338.148113084091));
#36162=CARTESIAN_POINT('Ctrl Pts',(101.295569847469,-3.69215585612748,338.252050276794));
#36163=CARTESIAN_POINT('Ctrl Pts',(101.287838139476,-3.59904841592456,338.352019326068));
#36164=CARTESIAN_POINT('Ctrl Pts',(101.280102061374,-3.50588834960681,338.452044879769));
#36165=CARTESIAN_POINT('Ctrl Pts',(101.272365983271,-3.4086355738239,338.54809754579));
#36166=CARTESIAN_POINT('Ctrl Pts',(101.264629905168,-3.30767761363785,338.639842285971));
#36167=CARTESIAN_POINT('Ctrl Pts',(101.256881904041,-3.2065640546801,338.731728425293));
#36168=CARTESIAN_POINT('Ctrl Pts',(101.249133902913,-3.1017342061043,338.819293123715));
#36169=CARTESIAN_POINT('Ctrl Pts',(101.241385901786,-2.99360752957126,338.902242563116));
#36170=CARTESIAN_POINT('Ctrl Pts',(101.235523480193,-2.91179492360666,338.965005148801));
#36171=CARTESIAN_POINT('Ctrl Pts',(101.229661058601,-2.82809554193822,339.025126363737));
#36172=CARTESIAN_POINT('Ctrl Pts',(101.223798637008,-2.74270074531183,339.082496256479));
#36173=CARTESIAN_POINT('Ctrl Pts',(101.21602355823,-2.62944528243802,339.158583489123));
#36174=CARTESIAN_POINT('Ctrl Pts',(101.208248479451,-2.51284226915805,339.230074531481));
#36175=CARTESIAN_POINT('Ctrl Pts',(101.200473400673,-2.39330127820999,339.29666057005));
#36176=CARTESIAN_POINT('Ctrl Pts',(101.192707889624,-2.27390739006172,339.363164670259));
#36177=CARTESIAN_POINT('Ctrl Pts',(101.184942378575,-2.15158305600174,339.424775588041));
#36178=CARTESIAN_POINT('Ctrl Pts',(101.177176867526,-2.02676786706079,339.481226960951));
#36179=CARTESIAN_POINT('Ctrl Pts',(101.169419056004,-1.90207643274323,339.53762236216));
#36180=CARTESIAN_POINT('Ctrl Pts',(101.161661244481,-1.77489941221519,339.588868238999));
#36181=CARTESIAN_POINT('Ctrl Pts',(101.153903432959,-1.64570179978444,339.634743644333));
#36182=CARTESIAN_POINT('Ctrl Pts',(101.146151459436,-1.51660141265351,339.680584526971));
#36183=CARTESIAN_POINT('Ctrl Pts',(101.138399485913,-1.38548382707886,339.721062852148));
#36184=CARTESIAN_POINT('Ctrl Pts',(101.13064751239,-1.25283453341215,339.756005539777));
#36185=CARTESIAN_POINT('Ctrl Pts',(101.122898821833,-1.12024141680033,339.790933429157));
#36186=CARTESIAN_POINT('Ctrl Pts',(101.115150131275,-0.98611825946724,339.820330244366));
#36187=CARTESIAN_POINT('Ctrl Pts',(101.107401440717,-0.850966041638258,
339.844072652064));
#36188=CARTESIAN_POINT('Ctrl Pts',(101.099654362339,-0.715841943357102,
339.867810119956));
#36189=CARTESIAN_POINT('Ctrl Pts',(101.091907283962,-0.579689595186712,
339.885895452785));
#36190=CARTESIAN_POINT('Ctrl Pts',(101.084160205584,-0.443020119450266,
339.898256448601));
#36191=CARTESIAN_POINT('Ctrl Pts',(101.076413062278,-0.306349498291885,
339.910617548014));
#36192=CARTESIAN_POINT('Ctrl Pts',(101.068665918972,-0.169162130208226,
339.917254179514));
#36193=CARTESIAN_POINT('Ctrl Pts',(101.060918775666,-0.031973813343201,
339.918146067144));
#36194=CARTESIAN_POINT('Ctrl Pts',(101.053169890638,0.105245346367392,339.919038155288));
#36195=CARTESIAN_POINT('Ctrl Pts',(101.04542100561,0.242465064494158,339.914182927));
#36196=CARTESIAN_POINT('Ctrl Pts',(101.037672120582,0.37917038748985,339.90361222771));
#36197=CARTESIAN_POINT('Ctrl Pts',(101.029915010807,0.516020810928358,339.893030308571));
#36198=CARTESIAN_POINT('Ctrl Pts',(101.022157901033,0.652355358254423,339.87672083029));
#36199=CARTESIAN_POINT('Ctrl Pts',(101.014400791258,0.787664485461182,339.854767524902));
#36200=CARTESIAN_POINT('Ctrl Pts',(101.006639536332,0.923045917539265,339.83280248837));
#36201=CARTESIAN_POINT('Ctrl Pts',(100.998878281406,1.0574004549784,339.805187693972));
#36202=CARTESIAN_POINT('Ctrl Pts',(100.99111702648,1.1902305522226,339.772057658396));
#36203=CARTESIAN_POINT('Ctrl Pts',(100.983343356075,1.32327313433306,339.73887462556));
#36204=CARTESIAN_POINT('Ctrl Pts',(100.97556968567,1.45478602802753,339.700158831844));
#36205=CARTESIAN_POINT('Ctrl Pts',(100.967796015265,1.58428775809218,339.656094432253));
#36206=CARTESIAN_POINT('Ctrl Pts',(100.960384211088,1.70776115146784,339.614081241064));
#36207=CARTESIAN_POINT('Ctrl Pts',(100.952972406911,1.82940613829515,339.56720629652));
#36208=CARTESIAN_POINT('Ctrl Pts',(100.945560602734,1.94882544889128,339.515668547652));
#36209=CARTESIAN_POINT('Ctrl Pts',(100.937785523955,2.07409785562988,339.46160478019));
#36210=CARTESIAN_POINT('Ctrl Pts',(100.930010445177,2.19731677950854,339.402238723881));
#36211=CARTESIAN_POINT('Ctrl Pts',(100.922235366399,2.31800088935477,339.337747680473));
#36212=CARTESIAN_POINT('Ctrl Pts',(100.91446985535,2.43853648972047,339.2733359974));
#36213=CARTESIAN_POINT('Ctrl Pts',(100.906704344301,2.55654314102322,339.203812058059));
#36214=CARTESIAN_POINT('Ctrl Pts',(100.898938833252,2.67155896547046,339.129401379924));
#36215=CARTESIAN_POINT('Ctrl Pts',(100.891181021729,2.78646075139305,339.055064480192));
#36216=CARTESIAN_POINT('Ctrl Pts',(100.883423210207,2.89837728573366,338.975850694872));
#36217=CARTESIAN_POINT('Ctrl Pts',(100.875665398685,3.0068711342323,338.892031480425));
#36218=CARTESIAN_POINT('Ctrl Pts',(100.867913425162,3.11528333766948,338.808275342595));
#36219=CARTESIAN_POINT('Ctrl Pts',(100.860161451639,3.22027767395822,338.719920912013));
#36220=CARTESIAN_POINT('Ctrl Pts',(100.852409478116,3.3214458696728,338.627282784308));
#36221=CARTESIAN_POINT('Ctrl Pts',(100.844660787558,3.42257122059623,338.534683888904));
#36222=CARTESIAN_POINT('Ctrl Pts',(100.836912097001,3.51987336607719,338.437805168009));
#36223=CARTESIAN_POINT('Ctrl Pts',(100.829163406443,3.61297748333231,338.337001163835));
#36224=CARTESIAN_POINT('Ctrl Pts',(100.821416328065,3.70606222949821,338.236218132776));
#36225=CARTESIAN_POINT('Ctrl Pts',(100.813669249687,3.79495041972273,338.131511729846));
#36226=CARTESIAN_POINT('Ctrl Pts',(100.805922171309,3.87930474022827,338.023272696093));
#36227=CARTESIAN_POINT('Ctrl Pts',(100.798175028004,3.96365976770414,337.915032755193));
#36228=CARTESIAN_POINT('Ctrl Pts',(100.790427884698,4.04348060939842,337.803260432722));
#36229=CARTESIAN_POINT('Ctrl Pts',(100.782680741392,4.11847108685283,337.688378501859));
#36230=CARTESIAN_POINT('Ctrl Pts',(100.774931856364,4.19347842375881,337.573470743098));
#36231=CARTESIAN_POINT('Ctrl Pts',(100.767182971336,4.2636530218539,337.455452312051));
#36232=CARTESIAN_POINT('Ctrl Pts',(100.759434086308,4.32874298972811,337.33477347753));
#36233=CARTESIAN_POINT('Ctrl Pts',(100.751676976533,4.39390204476664,337.213966553249));
#36234=CARTESIAN_POINT('Ctrl Pts',(100.743919866758,4.45396550296464,337.090493929296));
#36235=CARTESIAN_POINT('Ctrl Pts',(100.736162756984,4.50872803287847,336.964829404309));
#36236=CARTESIAN_POINT('Ctrl Pts',(100.728401502057,4.56351982613743,336.839097728217));
#36237=CARTESIAN_POINT('Ctrl Pts',(100.720640247131,4.61300490586243,336.71117218157));
#36238=CARTESIAN_POINT('Ctrl Pts',(100.712878992205,4.65702713955602,336.58154395574));
#36239=CARTESIAN_POINT('Ctrl Pts',(100.7051053218,4.70111979447662,336.451708366995));
#36240=CARTESIAN_POINT('Ctrl Pts',(100.697331651396,4.73973203056139,336.320165031491));
#36241=CARTESIAN_POINT('Ctrl Pts',(100.689557980991,4.77275815381855,336.187418488848));
#36242=CARTESIAN_POINT('Ctrl Pts',(100.682146176814,4.80424690309206,336.060851329704));
#36243=CARTESIAN_POINT('Ctrl Pts',(100.674734372637,4.83065784455062,335.933190742926));
#36244=CARTESIAN_POINT('Ctrl Pts',(100.66732256846,4.85194329325969,335.804878463802));
#36245=CARTESIAN_POINT('Ctrl Pts',(100.659547489682,4.87427200521635,335.670277217654));
#36246=CARTESIAN_POINT('Ctrl Pts',(100.651772410903,4.89103065195819,335.534533416312));
#36247=CARTESIAN_POINT('Ctrl Pts',(100.643997332125,4.90210785439088,335.398147769577));
#36248=CARTESIAN_POINT('Ctrl Pts',(100.636231821076,4.91317142562076,335.261929954063));
#36249=CARTESIAN_POINT('Ctrl Pts',(100.628466310027,4.91856743204089,335.125072250561));
#36250=CARTESIAN_POINT('Ctrl Pts',(100.620700798978,4.91823556752981,334.988085102406));
#36251=CARTESIAN_POINT('Ctrl Pts',(100.612942987456,4.91790403206337,334.851233777407));
#36252=CARTESIAN_POINT('Ctrl Pts',(100.605185175933,4.9118559285371,334.714253651524));
#36253=CARTESIAN_POINT('Ctrl Pts',(100.597427364411,4.90008280970267,334.577659473225));
#36254=CARTESIAN_POINT('Ctrl Pts',(100.589675390888,4.8883185505134,334.441168086376));
#36255=CARTESIAN_POINT('Ctrl Pts',(100.581923417365,4.87083788481801,334.305062456871));
#36256=CARTESIAN_POINT('Ctrl Pts',(100.574171443842,4.8476844226134,334.169856156289));
#36257=CARTESIAN_POINT('Ctrl Pts',(100.566422753285,4.82454076591387,334.034707115656));
#36258=CARTESIAN_POINT('Ctrl Pts',(100.558674062727,4.79572915681226,333.900457030895));
#36259=CARTESIAN_POINT('Ctrl Pts',(100.550925372169,4.76134489930317,333.767612961615));
#36260=CARTESIAN_POINT('Ctrl Pts',(100.543178293791,4.72696779572603,333.634796531653));
#36261=CARTESIAN_POINT('Ctrl Pts',(100.535431215414,4.68702044782326,333.503385913469));
#36262=CARTESIAN_POINT('Ctrl Pts',(100.527684137036,4.64164889823777,333.373876213818));
#36263=CARTESIAN_POINT('Ctrl Pts',(100.51993699373,4.596276968395,333.24436542875));
#36264=CARTESIAN_POINT('Ctrl Pts',(100.512189850424,4.54548087543105,333.116755962883));
#36265=CARTESIAN_POINT('Ctrl Pts',(100.504442707118,4.48945585917286,332.991525665825));
#36266=CARTESIAN_POINT('Ctrl Pts',(100.49669382209,4.43341824730153,332.866267214338));
#36267=CARTESIAN_POINT('Ctrl Pts',(100.488944937062,4.3721495324679,332.743389352755));
#36268=CARTESIAN_POINT('Ctrl Pts',(100.481196052034,4.30589204242829,332.623347568227));
#36269=CARTESIAN_POINT('Ctrl Pts',(100.473438942259,4.23956422600428,332.503178370109));
#36270=CARTESIAN_POINT('Ctrl Pts',(100.465681832485,4.16823724602133,332.385851605034));
#36271=CARTESIAN_POINT('Ctrl Pts',(100.45792472271,4.09219841323417,332.271796340222));
#36272=CARTESIAN_POINT('Ctrl Pts',(100.450163467784,4.01611894772591,332.157680127924));
#36273=CARTESIAN_POINT('Ctrl Pts',(100.442402212858,3.93532284247185,332.046839215009));
#36274=CARTESIAN_POINT('Ctrl Pts',(100.434640957931,3.85013865852148,331.93967070846));
#36275=CARTESIAN_POINT('Ctrl Pts',(100.426867287527,3.76481820763837,331.832330767227));
#36276=CARTESIAN_POINT('Ctrl Pts',(100.419093617122,3.67509590697439,331.728675267351));
#36277=CARTESIAN_POINT('Ctrl Pts',(100.411319946717,3.58133883757604,331.629066124504));
#36278=CARTESIAN_POINT('Ctrl Pts',(100.40390814254,3.49194618231444,331.53409381122));
#36279=CARTESIAN_POINT('Ctrl Pts',(100.396496338363,3.39888614725456,331.442799818424));
#36280=CARTESIAN_POINT('Ctrl Pts',(100.389084534186,3.3025043919707,331.355463293707));
#36281=CARTESIAN_POINT('Ctrl Pts',(100.381309455408,3.20139867975431,331.263846145752));
#36282=CARTESIAN_POINT('Ctrl Pts',(100.373534376629,3.0963178866018,331.176294682293));
#36283=CARTESIAN_POINT('Ctrl Pts',(100.365759297851,2.98762279644792,331.093173527191));
#36284=CARTESIAN_POINT('Ctrl Pts',(100.357993786802,2.87906146252249,331.010154657961));
#36285=CARTESIAN_POINT('Ctrl Pts',(100.350228275753,2.76689498861329,330.931555484785));
#36286=CARTESIAN_POINT('Ctrl Pts',(100.342462764704,2.65151998230749,330.857702950545));
#36287=CARTESIAN_POINT('Ctrl Pts',(100.334704953181,2.53625937065612,330.783923641307));
#36288=CARTESIAN_POINT('Ctrl Pts',(100.326947141659,2.41779688459907,330.714881814559));
#36289=CARTESIAN_POINT('Ctrl Pts',(100.319189330137,2.29656081581479,330.650863133705));
#36290=CARTESIAN_POINT('Ctrl Pts',(100.311437356614,2.17541598101747,330.586892628939));
#36291=CARTESIAN_POINT('Ctrl Pts',(100.303685383091,2.05150206223303,330.527937927792));
#36292=CARTESIAN_POINT('Ctrl Pts',(100.295933409568,1.92527453263051,330.474240280737));
#36293=CARTESIAN_POINT('Ctrl Pts',(100.288184719011,1.79910046046129,330.420565374667));
#36294=CARTESIAN_POINT('Ctrl Pts',(100.280436028453,1.67061508519094,330.372143247297));
#36295=CARTESIAN_POINT('Ctrl Pts',(100.272687337895,1.54029637852283,330.329168154514));
#36296=CARTESIAN_POINT('Ctrl Pts',(100.264940259517,1.41000478575017,330.286202003057));
#36297=CARTESIAN_POINT('Ctrl Pts',(100.25719318114,1.27788099126858,330.248680754309));
#36298=CARTESIAN_POINT('Ctrl Pts',(100.249446102762,1.14442037296369,330.216749528569));
#36299=CARTESIAN_POINT('Ctrl Pts',(100.241698959456,1.01095863613017,330.184818035214));
#36300=CARTESIAN_POINT('Ctrl Pts',(100.23395181615,0.876160433271687,330.158476749264));
#36301=CARTESIAN_POINT('Ctrl Pts',(100.226204672844,0.740533253792945,330.137820081226));
#36302=CARTESIAN_POINT('Ctrl Pts',(100.218455787816,0.604875582445456,330.117158769131));
#36303=CARTESIAN_POINT('Ctrl Pts',(100.210706902788,0.468388949961799,330.102184676912));
#36304=CARTESIAN_POINT('Ctrl Pts',(100.20295801776,0.331587522659386,330.092940516224));
#36305=CARTESIAN_POINT('Ctrl Pts',(100.195200907985,0.194640892907958,330.083686543688));
#36306=CARTESIAN_POINT('Ctrl Pts',(100.187443798211,0.0573791914896888,
330.08017467806));
#36307=CARTESIAN_POINT('Ctrl Pts',(100.179686688436,-0.0796812894812625,
330.082395506488));
#36308=CARTESIAN_POINT('Ctrl Pts',(100.17192543351,-0.216815011190714,330.084617521657));
#36309=CARTESIAN_POINT('Ctrl Pts',(100.164164178584,-0.353746908180597,
330.092578312245));
#36310=CARTESIAN_POINT('Ctrl Pts',(100.156402923657,-0.489965241480037,
330.106216481633));
#36311=CARTESIAN_POINT('Ctrl Pts',(100.148629253253,-0.62640147971949,330.119876467647));
#36312=CARTESIAN_POINT('Ctrl Pts',(100.140855582848,-0.762121486112149,
330.139231925682));
#36313=CARTESIAN_POINT('Ctrl Pts',(100.133081912443,-0.896622269431508,
330.164170022792));
#36314=CARTESIAN_POINT('Ctrl Pts',(100.125670108266,-1.02486200892952,330.187947245483));
#36315=CARTESIAN_POINT('Ctrl Pts',(100.118258304089,-1.15199319989853,330.216798996364));
#36316=CARTESIAN_POINT('Ctrl Pts',(100.110846499912,-1.2775940449448,330.250585665703));
#36317=CARTESIAN_POINT('Ctrl Pts',(100.103071421134,-1.40935096155144,330.286028320353));
#36318=CARTESIAN_POINT('Ctrl Pts',(100.095296342355,-1.53984010171249,330.327013880536));
#36319=CARTESIAN_POINT('Ctrl Pts',(100.087521263577,-1.66855960455591,330.373436274237));
#36320=CARTESIAN_POINT('Ctrl Pts',(100.079755752528,-1.79712070985586,330.419801542228));
#36321=CARTESIAN_POINT('Ctrl Pts',(100.071990241479,-1.92391614656229,330.47159020048));
#36322=CARTESIAN_POINT('Ctrl Pts',(100.06422473043,-2.0484563543082,330.528645660765));
#36323=CARTESIAN_POINT('Ctrl Pts',(100.056466918907,-2.17287308007527,330.585644550395));
#36324=CARTESIAN_POINT('Ctrl Pts',(100.048709107385,-2.29503867371132,330.647899688134));
#36325=CARTESIAN_POINT('Ctrl Pts',(100.040951295863,-2.41448114156284,330.715205503232));
#36326=CARTESIAN_POINT('Ctrl Pts',(100.03319932234,-2.53383372516972,330.782460668569));
#36327=CARTESIAN_POINT('Ctrl Pts',(100.025447348817,-2.65046692274143,330.854758754851));
#36328=CARTESIAN_POINT('Ctrl Pts',(100.017695375294,-2.76393137894123,330.931847299449));
#36329=CARTESIAN_POINT('Ctrl Pts',(100.009946684736,-2.87734778287708,331.008903197002));
#36330=CARTESIAN_POINT('Ctrl Pts',(100.002197994179,-2.98759779187196,331.090745298601));
#36331=CARTESIAN_POINT('Ctrl Pts',(99.9944493036212,-3.09425939409105,331.177076790651));
#36332=CARTESIAN_POINT('Ctrl Pts',(99.9867022252433,-3.20089880447274,331.263390320713));
#36333=CARTESIAN_POINT('Ctrl Pts',(99.9789551468655,-3.30395098948162,331.354191137564));
#36334=CARTESIAN_POINT('Ctrl Pts',(99.9712080684876,-3.40302583696322,331.449141200292));
#36335=CARTESIAN_POINT('Ctrl Pts',(99.9634609251818,-3.50210151478734,331.544092058794));
#36336=CARTESIAN_POINT('Ctrl Pts',(99.955713781876,-3.59719950639529,331.643191962081));
#36337=CARTESIAN_POINT('Ctrl Pts',(99.9479666385702,-3.68796578834079,331.746065242429));
#36338=CARTESIAN_POINT('Ctrl Pts',(99.9402177535422,-3.77875247647306,331.848961650874));
#36339=CARTESIAN_POINT('Ctrl Pts',(99.9324688685141,-3.8652052585162,331.955632831432));
#36340=CARTESIAN_POINT('Ctrl Pts',(99.924719983486,-3.94700997243212,332.065669524402));
#36341=CARTESIAN_POINT('Ctrl Pts',(99.9169628737113,-4.02890151471693,332.175823011456));
#36342=CARTESIAN_POINT('Ctrl Pts',(99.9092057639366,-4.10613490015827,332.289348832527));
#36343=CARTESIAN_POINT('Ctrl Pts',(99.9014486541619,-4.17843864893525,332.405807732726));
#36344=CARTESIAN_POINT('Ctrl Pts',(99.8936873992357,-4.2507810345239,332.522328864838));
#36345=CARTESIAN_POINT('Ctrl Pts',(99.8859261443095,-4.31818834249381,332.641785858909));
#36346=CARTESIAN_POINT('Ctrl Pts',(99.8781648893833,-4.38043527125306,332.763715157485));
#36347=CARTESIAN_POINT('Ctrl Pts',(99.8703912189787,-4.44278177481197,332.885839503202));
#36348=CARTESIAN_POINT('Ctrl Pts',(99.862617548574,-4.49995124029065,333.010443700996));
#36349=CARTESIAN_POINT('Ctrl Pts',(99.8548438781693,-4.55176635390703,333.137043714431));
#36350=CARTESIAN_POINT('Ctrl Pts',(99.8474320739922,-4.60116946151882,333.257750466784));
#36351=CARTESIAN_POINT('Ctrl Pts',(99.8400202698151,-4.64570539089723,333.380271135409));
#36352=CARTESIAN_POINT('Ctrl Pts',(99.832608465638,-4.68526328407162,333.504175471043));
#36353=CARTESIAN_POINT('Ctrl Pts',(99.8232353781635,-4.73528883576806,333.660866898474));
#36354=CARTESIAN_POINT('Ctrl Pts',(99.8138622906892,-4.7774827072035,333.820172031332));
#36355=CARTESIAN_POINT('Ctrl Pts',(99.8044892032148,-4.81161011964247,333.981377833024));
#36356=CARTESIAN_POINT('Ctrl Pts',(99.7948303774347,-4.84677790528113,334.147497989006));
#36357=CARTESIAN_POINT('Ctrl Pts',(99.7851715516546,-4.87337953316264,334.315636592827));
#36358=CARTESIAN_POINT('Ctrl Pts',(99.7755127258746,-4.89121119682611,334.484989232595));
#36359=CARTESIAN_POINT('Ctrl Pts',(99.7658539000946,-4.90904286048958,334.654341872363));
#36360=CARTESIAN_POINT('Ctrl Pts',(99.7561950743145,-4.91810436491552,334.824908550451));
#36361=CARTESIAN_POINT('Ctrl Pts',(99.7465362485345,-4.91824825774415,334.995860229885));
#36362=CARTESIAN_POINT('',(103.246536248441,-4.9182479760333,335.004461921597));
#36363=CARTESIAN_POINT('Ctrl Pts',(103.246536248441,-4.9182479760333,335.004461921597));
#36364=CARTESIAN_POINT('Ctrl Pts',(103.236856380282,-4.91809274950663,335.175563661959));
#36365=CARTESIAN_POINT('Ctrl Pts',(103.227176512124,-4.90900520981435,335.346267587011));
#36366=CARTESIAN_POINT('Ctrl Pts',(103.217496643965,-4.89113126270125,335.515769360787));
#36367=CARTESIAN_POINT('Ctrl Pts',(103.207644322872,-4.87293887998704,335.68829091519));
#36368=CARTESIAN_POINT('Ctrl Pts',(103.197792001779,-4.84564425788045,335.859567237283));
#36369=CARTESIAN_POINT('Ctrl Pts',(103.187939680686,-4.80944972616464,336.028774219153));
#36370=CARTESIAN_POINT('Ctrl Pts',(103.182448079432,-4.78927519735431,336.123088773558));
#36371=CARTESIAN_POINT('Ctrl Pts',(103.176956478179,-4.76633645145549,336.21676082811));
#36372=CARTESIAN_POINT('Ctrl Pts',(103.171464876925,-4.74067489486865,336.30965056548));
#36373=CARTESIAN_POINT('Ctrl Pts',(103.163689798147,-4.70434293724311,336.441165035016));
#36374=CARTESIAN_POINT('Ctrl Pts',(103.155914719368,-4.66247676530616,336.571374310764));
#36375=CARTESIAN_POINT('Ctrl Pts',(103.14813964059,-4.61518583907942,336.699777259896));
#36376=CARTESIAN_POINT('Ctrl Pts',(103.140374129541,-4.5679531073481,336.828022201025));
#36377=CARTESIAN_POINT('Ctrl Pts',(103.132608618492,-4.51530903746602,336.95446487499));
#36378=CARTESIAN_POINT('Ctrl Pts',(103.124843107443,-4.45741352141672,337.078616790462));
#36379=CARTESIAN_POINT('Ctrl Pts',(103.11708529592,-4.39957540894019,337.202645608948));
#36380=CARTESIAN_POINT('Ctrl Pts',(103.109327484398,-4.33649637630331,337.324387836976));
#36381=CARTESIAN_POINT('Ctrl Pts',(103.101569672876,-4.26838517821838,337.443372880439));
#36382=CARTESIAN_POINT('Ctrl Pts',(103.093817699353,-4.20032523596984,337.562268383884));
#36383=CARTESIAN_POINT('Ctrl Pts',(103.08606572583,-4.12724085924443,337.678410494829));
#36384=CARTESIAN_POINT('Ctrl Pts',(103.078313752307,-4.04938754062701,337.791351573757));
#36385=CARTESIAN_POINT('Ctrl Pts',(103.070565061749,-3.97156719293634,337.90424482207));
#36386=CARTESIAN_POINT('Ctrl Pts',(103.062816371192,-3.8889821416736,338.013939413484));
#36387=CARTESIAN_POINT('Ctrl Pts',(103.055067680634,-3.80193204465115,338.120015350981));
#36388=CARTESIAN_POINT('Ctrl Pts',(103.047320602256,-3.71490005912839,338.226069218493));
#36389=CARTESIAN_POINT('Ctrl Pts',(103.039573523878,-3.62340512347811,338.328505627676));
#36390=CARTESIAN_POINT('Ctrl Pts',(103.0318264455,-3.52778790638298,338.426936758984));
#36391=CARTESIAN_POINT('Ctrl Pts',(103.024079302195,-3.43216988792355,338.525368715241));
#36392=CARTESIAN_POINT('Ctrl Pts',(103.016332158889,-3.3324297914626,338.6197950463));
#36393=CARTESIAN_POINT('Ctrl Pts',(103.008585015583,-3.2289456678323,338.709864274699));
#36394=CARTESIAN_POINT('Ctrl Pts',(103.000836130555,-3.12543827877412,338.799953752572));
#36395=CARTESIAN_POINT('Ctrl Pts',(102.993087245527,-3.01818548236551,338.885683921983));
#36396=CARTESIAN_POINT('Ctrl Pts',(102.985338360499,-2.90759865135431,338.966743392903));
#36397=CARTESIAN_POINT('Ctrl Pts',(102.977581250724,-2.79689444233794,339.047888901184));
#36398=CARTESIAN_POINT('Ctrl Pts',(102.969824140949,-2.68284944542831,339.124353576403));
#36399=CARTESIAN_POINT('Ctrl Pts',(102.962067031174,-2.56590473952805,339.195868912415));
#36400=CARTESIAN_POINT('Ctrl Pts',(102.954305776248,-2.44889754211613,339.267422463935));
#36401=CARTESIAN_POINT('Ctrl Pts',(102.946544521322,-2.32898788970553,339.334021216618));
#36402=CARTESIAN_POINT('Ctrl Pts',(102.938783266396,-2.20664085124335,339.395443005673));
#36403=CARTESIAN_POINT('Ctrl Pts',(102.931009595991,-2.08409809739251,339.456963049574));
#36404=CARTESIAN_POINT('Ctrl Pts',(102.923235925587,-1.95911052263342,339.513289420368));
#36405=CARTESIAN_POINT('Ctrl Pts',(102.915462255182,-1.83216335023625,339.564248078331));
#36406=CARTESIAN_POINT('Ctrl Pts',(102.908050451005,-1.71112559925907,339.612834598505));
#36407=CARTESIAN_POINT('Ctrl Pts',(102.900638646828,-1.58830685465758,339.656541797219));
#36408=CARTESIAN_POINT('Ctrl Pts',(102.893226842651,-1.46413810480163,339.695261725673));
#36409=CARTESIAN_POINT('Ctrl Pts',(102.885451763873,-1.33388347463229,339.735879433162));
#36410=CARTESIAN_POINT('Ctrl Pts',(102.877676685094,-1.20173152884744,339.771136986518));
#36411=CARTESIAN_POINT('Ctrl Pts',(102.869901606316,-1.06816291583152,339.800855241282));
#36412=CARTESIAN_POINT('Ctrl Pts',(102.862136095267,-0.934758667497211,
339.830536925841));
#36413=CARTESIAN_POINT('Ctrl Pts',(102.854370584218,-0.799941598494425,
339.854692790527));
#36414=CARTESIAN_POINT('Ctrl Pts',(102.846605073169,-0.664209018331135,
339.873192941231));
#36415=CARTESIAN_POINT('Ctrl Pts',(102.838847261647,-0.528611017416344,
339.891674748983));
#36416=CARTESIAN_POINT('Ctrl Pts',(102.831089450124,-0.392099696577586,
339.90451194986));
#36417=CARTESIAN_POINT('Ctrl Pts',(102.823331638602,-0.25518375759123,339.91162542468));
#36418=CARTESIAN_POINT('Ctrl Pts',(102.815579665079,-0.118370852191,339.918733546385));
#36419=CARTESIAN_POINT('Ctrl Pts',(102.807827691556,0.0188456765122954,
339.920126495275));
#36420=CARTESIAN_POINT('Ctrl Pts',(102.800075718033,0.155951137200529,339.915776877087));
#36421=CARTESIAN_POINT('Ctrl Pts',(102.792327027475,0.292998533644854,339.911429100966));
#36422=CARTESIAN_POINT('Ctrl Pts',(102.784578336918,0.429934565763458,339.901343607172));
#36423=CARTESIAN_POINT('Ctrl Pts',(102.77682964636,0.566243887067581,339.885545099869));
#36424=CARTESIAN_POINT('Ctrl Pts',(102.769082567982,0.70252484807893,339.869749879578));
#36425=CARTESIAN_POINT('Ctrl Pts',(102.761335489605,0.838178969604223,339.84824405504));
#36426=CARTESIAN_POINT('Ctrl Pts',(102.753588411227,0.9726957705425,339.821104230409));
#36427=CARTESIAN_POINT('Ctrl Pts',(102.745841267921,1.10721369886104,339.793964178321));
#36428=CARTESIAN_POINT('Ctrl Pts',(102.738094124615,1.24059390442689,339.761190109263));
#36429=CARTESIAN_POINT('Ctrl Pts',(102.730346981309,1.37233623734387,339.722909729624));
#36430=CARTESIAN_POINT('Ctrl Pts',(102.722598096281,1.50410818873425,339.684620743742));
#36431=CARTESIAN_POINT('Ctrl Pts',(102.714849211253,1.63424115946567,339.640823092968));
#36432=CARTESIAN_POINT('Ctrl Pts',(102.707100326225,1.76225067762179,339.591694198411));
#36433=CARTESIAN_POINT('Ctrl Pts',(102.69934321645,1.89039606640315,339.542513157937));
#36434=CARTESIAN_POINT('Ctrl Pts',(102.691586106676,2.01641313482551,339.487989710296));
#36435=CARTESIAN_POINT('Ctrl Pts',(102.683828996901,2.13983739723886,339.428349464064));
#36436=CARTESIAN_POINT('Ctrl Pts',(102.676067741975,2.2633276136317,339.368677347991));
#36437=CARTESIAN_POINT('Ctrl Pts',(102.668306487049,2.38422191891857,339.303883169632));
#36438=CARTESIAN_POINT('Ctrl Pts',(102.660545232122,2.50208181449505,339.234237789269));
#36439=CARTESIAN_POINT('Ctrl Pts',(102.652771561718,2.62013024749392,339.164480998995));
#36440=CARTESIAN_POINT('Ctrl Pts',(102.644997891313,2.73513424285291,339.089857712131));
#36441=CARTESIAN_POINT('Ctrl Pts',(102.637224220908,2.84668486470064,339.010681780394));
#36442=CARTESIAN_POINT('Ctrl Pts',(102.629812416731,2.95304277826437,338.935191507328));
#36443=CARTESIAN_POINT('Ctrl Pts',(102.622400612554,3.0562613641603,338.85556307791));
#36444=CARTESIAN_POINT('Ctrl Pts',(102.614988808377,3.15601661340184,338.772100502165));
#36445=CARTESIAN_POINT('Ctrl Pts',(102.607213729599,3.26066116456381,338.684547176961));
#36446=CARTESIAN_POINT('Ctrl Pts',(102.59943865082,3.36182499410937,338.592497671611));
#36447=CARTESIAN_POINT('Ctrl Pts',(102.591663572042,3.45909734921933,338.49625922825));
#36448=CARTESIAN_POINT('Ctrl Pts',(102.583898060993,3.55625000450366,338.400139212421));
#36449=CARTESIAN_POINT('Ctrl Pts',(102.576132549944,3.64952043829995,338.299840787345));
#36450=CARTESIAN_POINT('Ctrl Pts',(102.568367038895,3.73853029717096,338.195711858043));
#36451=CARTESIAN_POINT('Ctrl Pts',(102.560609227373,3.82745190250776,338.091686172877));
#36452=CARTESIAN_POINT('Ctrl Pts',(102.55285141585,3.91212108731851,337.983837836835));
#36453=CARTESIAN_POINT('Ctrl Pts',(102.545093604328,3.99219603087451,337.872551812165));
#36454=CARTESIAN_POINT('Ctrl Pts',(102.537341630805,4.07221071549611,337.761349533756));
#36455=CARTESIAN_POINT('Ctrl Pts',(102.529589657282,4.14763781309923,337.646715031955));
#36456=CARTESIAN_POINT('Ctrl Pts',(102.521837683759,4.2181757582583,337.529066297063));
#36457=CARTESIAN_POINT('Ctrl Pts',(102.514088993202,4.28868383055571,337.411467386481));
#36458=CARTESIAN_POINT('Ctrl Pts',(102.506340302644,4.35430666802759,337.290857116273));
#36459=CARTESIAN_POINT('Ctrl Pts',(102.498591612086,4.41478616137502,337.167682221137));
#36460=CARTESIAN_POINT('Ctrl Pts',(102.490844533709,4.47525307145877,337.044532953566));
#36461=CARTESIAN_POINT('Ctrl Pts',(102.483097455331,4.5305785937871,336.91882047306));
#36462=CARTESIAN_POINT('Ctrl Pts',(102.475350376953,4.58055089581245,336.79101550897));
#36463=CARTESIAN_POINT('Ctrl Pts',(102.467603233647,4.63052361665375,336.663209473752));
#36464=CARTESIAN_POINT('Ctrl Pts',(102.459856090341,4.67514288536555,336.533311284007));
#36465=CARTESIAN_POINT('Ctrl Pts',(102.452108947036,4.71424543316517,336.401810635707));
#36466=CARTESIAN_POINT('Ctrl Pts',(102.444360062008,4.7533567720477,336.270280423269));
#36467=CARTESIAN_POINT('Ctrl Pts',(102.436611176979,4.7869488106213,336.137147409974));
#36468=CARTESIAN_POINT('Ctrl Pts',(102.428862291951,4.81490857052794,336.002915011333));
#36469=CARTESIAN_POINT('Ctrl Pts',(102.421105182177,4.84289800721261,335.868540137037));
#36470=CARTESIAN_POINT('Ctrl Pts',(102.413348072402,4.86524314346552,335.733063929671));
#36471=CARTESIAN_POINT('Ctrl Pts',(102.405590962627,4.88188233851452,335.596999074874));
#36472=CARTESIAN_POINT('Ctrl Pts',(102.397829707701,4.89853042501733,335.460861511368));
#36473=CARTESIAN_POINT('Ctrl Pts',(102.390068452775,4.9094664636159,335.324135063086));
#36474=CARTESIAN_POINT('Ctrl Pts',(102.382307197849,4.91468092974551,335.1873350509));
#36475=CARTESIAN_POINT('Ctrl Pts',(102.374533527444,4.91990373732155,335.050316203277));
#36476=CARTESIAN_POINT('Ctrl Pts',(102.366759857039,4.91938668419584,334.913223947672));
#36477=CARTESIAN_POINT('Ctrl Pts',(102.358986186635,4.91317239630912,334.776572010155));
#36478=CARTESIAN_POINT('Ctrl Pts',(102.351574382458,4.90724738501865,334.646281253207));
#36479=CARTESIAN_POINT('Ctrl Pts',(102.344162578281,4.89614363943262,334.516391030021));
#36480=CARTESIAN_POINT('Ctrl Pts',(102.336750774104,4.87994146821236,334.387338323933));
#36481=CARTESIAN_POINT('Ctrl Pts',(102.328975695325,4.8629451803167,334.251960360291));
#36482=CARTESIAN_POINT('Ctrl Pts',(102.321200616547,4.84028434042474,334.117076268646));
#36483=CARTESIAN_POINT('Ctrl Pts',(102.313425537768,4.81199503308198,333.983197726156));
#36484=CARTESIAN_POINT('Ctrl Pts',(102.305660026719,4.78374053753292,333.849483929736));
#36485=CARTESIAN_POINT('Ctrl Pts',(102.29789451567,4.74987143569738,333.716773599188));
#36486=CARTESIAN_POINT('Ctrl Pts',(102.290129004621,4.71047553957375,333.58557317136));
#36487=CARTESIAN_POINT('Ctrl Pts',(102.282371193099,4.67111870459582,333.454502829137));
#36488=CARTESIAN_POINT('Ctrl Pts',(102.274613381577,4.62624609219297,333.324939782324));
#36489=CARTESIAN_POINT('Ctrl Pts',(102.266855570055,4.57599644652163,333.197379800423));
#36490=CARTESIAN_POINT('Ctrl Pts',(102.259103596532,4.52578461530216,333.069915811455));
#36491=CARTESIAN_POINT('Ctrl Pts',(102.251351623009,4.47020394763686,332.944452249263));
#36492=CARTESIAN_POINT('Ctrl Pts',(102.243599649486,4.40944274613266,332.821468905184));
#36493=CARTESIAN_POINT('Ctrl Pts',(102.235850958928,4.34870727703337,332.698537644625));
#36494=CARTESIAN_POINT('Ctrl Pts',(102.22810226837,4.28279581050217,332.578084862768));
#36495=CARTESIAN_POINT('Ctrl Pts',(102.220353577813,4.21194433752394,332.460569363007));
#36496=CARTESIAN_POINT('Ctrl Pts',(102.212606499435,4.14110760578643,332.343078313326));
#36497=CARTESIAN_POINT('Ctrl Pts',(102.204859421057,4.06533311368053,332.2285236647));
#36498=CARTESIAN_POINT('Ctrl Pts',(102.197112342679,3.98490207281434,332.117338290298));
#36499=CARTESIAN_POINT('Ctrl Pts',(102.189365199373,3.90447035785861,332.006151984056));
#36500=CARTESIAN_POINT('Ctrl Pts',(102.181618056068,3.81938224539899,331.898335325059));
#36501=CARTESIAN_POINT('Ctrl Pts',(102.173870912762,3.72996117711833,331.794290612097));
#36502=CARTESIAN_POINT('Ctrl Pts',(102.166122027734,3.64052000508312,331.690222507675));
#36503=CARTESIAN_POINT('Ctrl Pts',(102.158373142706,3.54674419351778,331.589928333119));
#36504=CARTESIAN_POINT('Ctrl Pts',(102.150624257677,3.4489959361942,331.49377552136));
#36505=CARTESIAN_POINT('Ctrl Pts',(102.142867147903,3.35114392786029,331.397520652013));
#36506=CARTESIAN_POINT('Ctrl Pts',(102.135110038128,3.24931133021835,331.305416200796));
#36507=CARTESIAN_POINT('Ctrl Pts',(102.127352928353,3.14389591420087,331.217791446367));
#36508=CARTESIAN_POINT('Ctrl Pts',(102.119591673427,3.03842416755553,331.130119868071));
#36509=CARTESIAN_POINT('Ctrl Pts',(102.111830418501,2.92936609825969,331.046932993376));
#36510=CARTESIAN_POINT('Ctrl Pts',(102.104069163575,2.81714989634082,330.968517701385));
#36511=CARTESIAN_POINT('Ctrl Pts',(102.09629549317,2.70475418507014,330.889976970482));
#36512=CARTESIAN_POINT('Ctrl Pts',(102.088521822765,2.58919057548164,330.816223285626));
#36513=CARTESIAN_POINT('Ctrl Pts',(102.080748152361,2.47091413813151,330.747498808409));
#36514=CARTESIAN_POINT('Ctrl Pts',(102.073336348184,2.35814349739529,330.681973472141));
#36515=CARTESIAN_POINT('Ctrl Pts',(102.065924544006,2.24290716376067,330.621019795825));
#36516=CARTESIAN_POINT('Ctrl Pts',(102.058512739829,2.12561606546375,330.564806722955));
#36517=CARTESIAN_POINT('Ctrl Pts',(102.050737661051,2.00257618104758,330.505838479934));
#36518=CARTESIAN_POINT('Ctrl Pts',(102.042962582272,1.87688619001357,330.45190094201));
#36519=CARTESIAN_POINT('Ctrl Pts',(102.035187503494,1.74899590001713,330.40324066279));
#36520=CARTESIAN_POINT('Ctrl Pts',(102.027421992445,1.62126298716442,330.354640263142));
#36521=CARTESIAN_POINT('Ctrl Pts',(102.019656481396,1.49133552454444,330.311304338665));
#36522=CARTESIAN_POINT('Ctrl Pts',(102.011890970347,1.35968690581637,330.273433108412));
#36523=CARTESIAN_POINT('Ctrl Pts',(102.004133158825,1.22816881707706,330.235599427595));
#36524=CARTESIAN_POINT('Ctrl Pts',(101.996375347303,1.09493334154405,330.203219765723));
#36525=CARTESIAN_POINT('Ctrl Pts',(101.98861753578,0.960472464794403,330.176445739201));
#36526=CARTESIAN_POINT('Ctrl Pts',(101.980865562257,0.826112774118606,330.149691860983));
#36527=CARTESIAN_POINT('Ctrl Pts',(101.973113588735,0.690529899532061,330.128535297584));
#36528=CARTESIAN_POINT('Ctrl Pts',(101.965361615212,0.554229209151167,330.113077343949));
#36529=CARTESIAN_POINT('Ctrl Pts',(101.957612924654,0.417986242193478,330.097625936766));
#36530=CARTESIAN_POINT('Ctrl Pts',(101.949864234096,0.281026451643177,330.08786838329));
#36531=CARTESIAN_POINT('Ctrl Pts',(101.942115543539,0.143863363325315,330.083854518508));
#36532=CARTESIAN_POINT('Ctrl Pts',(101.934368465161,0.00672881293358724,
330.079841488845));
#36533=CARTESIAN_POINT('Ctrl Pts',(101.926621386783,-0.130608560630653,
330.081569782318));
#36534=CARTESIAN_POINT('Ctrl Pts',(101.918874308405,-0.267632565345737,
330.089037174599));
#36535=CARTESIAN_POINT('Ctrl Pts',(101.911127165099,-0.404657718453866,
330.096504629465));
#36536=CARTESIAN_POINT('Ctrl Pts',(101.903380021794,-0.541369107179274,
330.109711257805));
#36537=CARTESIAN_POINT('Ctrl Pts',(101.895632878488,-0.677253397031937,
330.128602777569));
#36538=CARTESIAN_POINT('Ctrl Pts',(101.88788399346,-0.813168236557865,330.147498544548));
#36539=CARTESIAN_POINT('Ctrl Pts',(101.880135108432,-0.948255220117501,
330.172081692381));
#36540=CARTESIAN_POINT('Ctrl Pts',(101.872386223404,-1.08200936168753,330.202246483643));
#36541=CARTESIAN_POINT('Ctrl Pts',(101.864629113629,-1.21590547128545,330.232443292125));
#36542=CARTESIAN_POINT('Ctrl Pts',(101.856872003854,-1.34846553101308,330.26823349248));
#36543=CARTESIAN_POINT('Ctrl Pts',(101.849114894079,-1.47919738674698,330.309460782219));
#36544=CARTESIAN_POINT('Ctrl Pts',(101.841353639153,-1.60999910140449,330.350710102504));
#36545=CARTESIAN_POINT('Ctrl Pts',(101.833592384227,-1.73897029809642,330.397402168467));
#36546=CARTESIAN_POINT('Ctrl Pts',(101.825831129301,-1.86563801587126,330.449332152724));
#36547=CARTESIAN_POINT('Ctrl Pts',(101.818057458896,-1.99250836071363,330.501345208031));
#36548=CARTESIAN_POINT('Ctrl Pts',(101.810283788492,-2.11706750796173,330.558612761914));
#36549=CARTESIAN_POINT('Ctrl Pts',(101.802510118087,-2.23886555397652,330.620883183367));
#36550=CARTESIAN_POINT('Ctrl Pts',(101.79509831391,-2.35499387164689,330.68025490172));
#36551=CARTESIAN_POINT('Ctrl Pts',(101.787686509733,-2.46861211083911,330.744174061358));
#36552=CARTESIAN_POINT('Ctrl Pts',(101.780274705556,-2.57935582651927,330.812386528976));
#36553=CARTESIAN_POINT('Ctrl Pts',(101.772499626777,-2.69552742159293,330.883942292826));
#36554=CARTESIAN_POINT('Ctrl Pts',(101.764724547999,-2.8089027141783,330.96044899106));
#36555=CARTESIAN_POINT('Ctrl Pts',(101.75694946922,-2.91903095535628,331.041661795125));
#36556=CARTESIAN_POINT('Ctrl Pts',(101.749183958171,-3.02902367672238,331.122774661665));
#36557=CARTESIAN_POINT('Ctrl Pts',(101.741418447122,-3.13577698540662,331.208581881513));
#36558=CARTESIAN_POINT('Ctrl Pts',(101.733652936073,-3.23886633246278,331.298793717862));
#36559=CARTESIAN_POINT('Ctrl Pts',(101.725895124551,-3.34185346613127,331.388916108912));
#36560=CARTESIAN_POINT('Ctrl Pts',(101.718137313029,-3.44118357545025,331.483434169758));
#36561=CARTESIAN_POINT('Ctrl Pts',(101.710379501507,-3.53646292132437,331.58201622757));
#36562=CARTESIAN_POINT('Ctrl Pts',(101.702627527984,-3.63167056646917,331.680524099256));
#36563=CARTESIAN_POINT('Ctrl Pts',(101.694875554461,-3.72283324516891,331.783089600612));
#36564=CARTESIAN_POINT('Ctrl Pts',(101.687123580938,-3.80959229265892,331.889342573311));
#36565=CARTESIAN_POINT('Ctrl Pts',(101.67937489038,-3.89631459764081,331.995550547814));
#36566=CARTESIAN_POINT('Ctrl Pts',(101.671626199822,-3.97863673394537,332.105442585522));
#36567=CARTESIAN_POINT('Ctrl Pts',(101.663877509265,-4.05623889597741,332.218613820186));
#36568=CARTESIAN_POINT('Ctrl Pts',(101.656130430887,-4.13382491223149,332.331761508629));
#36569=CARTESIAN_POINT('Ctrl Pts',(101.648383352509,-4.20669268663047,332.448186714792));
#36570=CARTESIAN_POINT('Ctrl Pts',(101.640636274131,-4.2745647485384,332.567454158078));
#36571=CARTESIAN_POINT('Ctrl Pts',(101.632889130825,-4.34243737927953,332.68672260094));
#36572=CARTESIAN_POINT('Ctrl Pts',(101.62514198752,-4.4053140206942,332.80883298872));
#36573=CARTESIAN_POINT('Ctrl Pts',(101.617394844214,-4.4629625249699,332.93332427236));
#36574=CARTESIAN_POINT('Ctrl Pts',(101.609645959186,-4.52062398985323,333.057843544285));
#36575=CARTESIAN_POINT('Ctrl Pts',(101.601897074158,-4.573054814475,333.184744422588));
#36576=CARTESIAN_POINT('Ctrl Pts',(101.59414818913,-4.62007063878045,333.31354503316));
#36577=CARTESIAN_POINT('Ctrl Pts',(101.586391079355,-4.66713636616762,333.442482354031));
#36578=CARTESIAN_POINT('Ctrl Pts',(101.57863396958,-4.7087754777521,333.573323067354));
#36579=CARTESIAN_POINT('Ctrl Pts',(101.570876859805,-4.74485307879436,333.705568725982));
#36580=CARTESIAN_POINT('Ctrl Pts',(101.563115604879,-4.78094995855313,333.837885052462));
#36581=CARTESIAN_POINT('Ctrl Pts',(101.555354349953,-4.81147931904884,333.971607439323));
#36582=CARTESIAN_POINT('Ctrl Pts',(101.547593095027,-4.83635745769027,334.10622731976));
#36583=CARTESIAN_POINT('Ctrl Pts',(101.539819424622,-4.86127539324571,334.241062548133));
#36584=CARTESIAN_POINT('Ctrl Pts',(101.532045754218,-4.88052398721385,334.376797751824));
#36585=CARTESIAN_POINT('Ctrl Pts',(101.524272083813,-4.89407137280176,334.51291842529));
#36586=CARTESIAN_POINT('Ctrl Pts',(101.516860279636,-4.9069881243313,334.642702648657));
#36587=CARTESIAN_POINT('Ctrl Pts',(101.509448475459,-4.91472248797685,334.772836974893));
#36588=CARTESIAN_POINT('Ctrl Pts',(101.502036671282,-4.91729094773511,334.902877408281));
#36589=CARTESIAN_POINT('Ctrl Pts',(101.500203197018,-4.91792631326182,334.935045795652));
#36590=CARTESIAN_POINT('Ctrl Pts',(101.498369722754,-4.91824601993271,334.967220438261));
#36591=CARTESIAN_POINT('Ctrl Pts',(101.49653624849,-4.91824996307017,334.999397289198));
#36592=CARTESIAN_POINT('',(104.996536248525,-4.91824974554793,334.998417938773));
#36593=CARTESIAN_POINT('Ctrl Pts',(104.99653624849,-4.91824974554813,334.99841793939));
#36594=CARTESIAN_POINT('Ctrl Pts',(104.988593885279,-4.91829509434603,335.139396554485));
#36595=CARTESIAN_POINT('Ctrl Pts',(104.980651522069,-4.91227449297855,335.280324386072));
#36596=CARTESIAN_POINT('Ctrl Pts',(104.972709158858,-4.90022731154389,335.420660620571));
#36597=CARTESIAN_POINT('Ctrl Pts',(104.964761972148,-4.88817281370081,335.561082083073));
#36598=CARTESIAN_POINT('Ctrl Pts',(104.956814785438,-4.87008447169581,335.700910871338));
#36599=CARTESIAN_POINT('Ctrl Pts',(104.948867598728,-4.84605336641541,335.839612906257));
#36600=CARTESIAN_POINT('Ctrl Pts',(104.940914261939,-4.82200366421589,335.978422278334));
#36601=CARTESIAN_POINT('Ctrl Pts',(104.932960925151,-4.79200209388668,336.116102802447));
#36602=CARTESIAN_POINT('Ctrl Pts',(104.925007588362,-4.75619049114916,336.252132211231));
#36603=CARTESIAN_POINT('Ctrl Pts',(104.917041026786,-4.72031934097304,336.388387809357));
#36604=CARTESIAN_POINT('Ctrl Pts',(104.90907446521,-4.67861894877477,336.522986456037));
#36605=CARTESIAN_POINT('Ctrl Pts',(104.901107903634,-4.6312808721615,336.65542156131));
#36606=CARTESIAN_POINT('Ctrl Pts',(104.893134004349,-4.58389919417668,336.787978647717));
#36607=CARTESIAN_POINT('Ctrl Pts',(104.885160105064,-4.53086961314969,336.918367884027));
#36608=CARTESIAN_POINT('Ctrl Pts',(104.877186205779,-4.47243101695501,337.046104557709));
#36609=CARTESIAN_POINT('Ctrl Pts',(104.86919775366,-4.41388576689024,337.174074358323));
#36610=CARTESIAN_POINT('Ctrl Pts',(104.861209301541,-4.34991194027478,337.299381600503));
#36611=CARTESIAN_POINT('Ctrl Pts',(104.853220849422,-4.28079390098626,337.421566980238));
#36612=CARTESIAN_POINT('Ctrl Pts',(104.849111593804,-4.2452396175053,337.484419076059));
#36613=CARTESIAN_POINT('Ctrl Pts',(104.845002338186,-4.20832483760696,337.546445589308));
#36614=CARTESIAN_POINT('Ctrl Pts',(104.840893082569,-4.17009252427013,337.607587275917));
#36615=CARTESIAN_POINT('Ctrl Pts',(104.83311800379,-4.09775357149106,337.723272809814));
#36616=CARTESIAN_POINT('Ctrl Pts',(104.825342925012,-4.02048268832412,337.836128657948));
#36617=CARTESIAN_POINT('Ctrl Pts',(104.817567846234,-3.93852774286272,337.945705735677));
#36618=CARTESIAN_POINT('Ctrl Pts',(104.809802335185,-3.85667364817927,338.055147971836));
#36619=CARTESIAN_POINT('Ctrl Pts',(104.802036824136,-3.77014719185178,338.161319155537));
#36620=CARTESIAN_POINT('Ctrl Pts',(104.794271313087,-3.6792409722076,338.263796704902));
#36621=CARTESIAN_POINT('Ctrl Pts',(104.786513501564,-3.58842488634493,338.366172647478));
#36622=CARTESIAN_POINT('Ctrl Pts',(104.778755690042,-3.49323793679871,338.464861953279));
#36623=CARTESIAN_POINT('Ctrl Pts',(104.77099787852,-3.39401444881945,338.559473132881));
#36624=CARTESIAN_POINT('Ctrl Pts',(104.763245904997,-3.29486562966159,338.65401311457));
#36625=CARTESIAN_POINT('Ctrl Pts',(104.755493931474,-3.19168660005859,338.744480809944));
#36626=CARTESIAN_POINT('Ctrl Pts',(104.747741957951,-3.08484993292376,338.830520063104));
#36627=CARTESIAN_POINT('Ctrl Pts',(104.739993267393,-2.97805851118067,338.916522878589));
#36628=CARTESIAN_POINT('Ctrl Pts',(104.732244576836,-2.86761283657499,338.99810073734));
#36629=CARTESIAN_POINT('Ctrl Pts',(104.724495886278,-2.7539199266321,339.074936576218));
#36630=CARTESIAN_POINT('Ctrl Pts',(104.7167488079,-2.6402506714487,339.151756428758));
#36631=CARTESIAN_POINT('Ctrl Pts',(104.709001729522,-2.52333584842224,339.223836005148));
#36632=CARTESIAN_POINT('Ctrl Pts',(104.701254651145,-2.40361260272703,339.290900781714));
#36633=CARTESIAN_POINT('Ctrl Pts',(104.693507507839,-2.28388835363571,339.357966120347));
#36634=CARTESIAN_POINT('Ctrl Pts',(104.685760364533,-2.16135597594495,339.420016384302));
#36635=CARTESIAN_POINT('Ctrl Pts',(104.678013221227,-2.03647807651427,339.476822545777));
#36636=CARTESIAN_POINT('Ctrl Pts',(104.670264336199,-1.91157210188065,339.533641478483));
#36637=CARTESIAN_POINT('Ctrl Pts',(104.662515451171,-1.78431991191573,339.585213800845));
#36638=CARTESIAN_POINT('Ctrl Pts',(104.654766566143,-1.65520461521616,339.631358412417));
#36639=CARTESIAN_POINT('Ctrl Pts',(104.647009456368,-1.52595227420649,339.677552002357));
#36640=CARTESIAN_POINT('Ctrl Pts',(104.639252346594,-1.39483324483411,339.718306241558));
#36641=CARTESIAN_POINT('Ctrl Pts',(104.631495236819,-1.26234687418126,339.753489605726));
#36642=CARTESIAN_POINT('Ctrl Pts',(104.623733981893,-1.12978970704803,339.788691770758));
#36643=CARTESIAN_POINT('Ctrl Pts',(104.615972726966,-0.995864124176255,
339.81831704464));
#36644=CARTESIAN_POINT('Ctrl Pts',(104.60821147204,-0.861079246236491,339.842285162421));
#36645=CARTESIAN_POINT('Ctrl Pts',(104.600437801636,-0.726078756418496,
339.866291621379));
#36646=CARTESIAN_POINT('Ctrl Pts',(104.592664131231,-0.590216612258507,
339.88462278815));
#36647=CARTESIAN_POINT('Ctrl Pts',(104.584890460826,-0.454007522842867,
339.897250272521));
#36648=CARTESIAN_POINT('Ctrl Pts',(104.577478656649,-0.324138999309171,
339.909289944456));
#36649=CARTESIAN_POINT('Ctrl Pts',(104.570066852472,-0.193955391616291,
339.916144981575));
#36650=CARTESIAN_POINT('Ctrl Pts',(104.562655048295,-0.0639005739877349,
339.917834867006));
#36651=CARTESIAN_POINT('Ctrl Pts',(104.554879969517,0.0725286176657191,
339.919607578757));
#36652=CARTESIAN_POINT('Ctrl Pts',(104.547104890738,0.20924721671919,339.915701619692));
#36653=CARTESIAN_POINT('Ctrl Pts',(104.53932981196,0.345743442668588,339.906082401912));
#36654=CARTESIAN_POINT('Ctrl Pts',(104.531564300911,0.482071701322272,339.896475021192));
#36655=CARTESIAN_POINT('Ctrl Pts',(104.523798789862,0.618177745165577,339.881168397707));
#36656=CARTESIAN_POINT('Ctrl Pts',(104.516033278813,0.753547874336392,339.860179900331));
#36657=CARTESIAN_POINT('Ctrl Pts',(104.508275467291,0.888783783630108,339.839212213111));
#36658=CARTESIAN_POINT('Ctrl Pts',(104.500517655768,1.02328484654803,339.812573922674));
#36659=CARTESIAN_POINT('Ctrl Pts',(104.492759844246,1.15654092870476,339.780334312863));
#36660=CARTESIAN_POINT('Ctrl Pts',(104.485007870723,1.28969673143379,339.74811896438));
#36661=CARTESIAN_POINT('Ctrl Pts',(104.4772558972,1.42160903984659,339.710310778161));
#36662=CARTESIAN_POINT('Ctrl Pts',(104.469503923677,1.55177673426961,339.667030322323));
#36663=CARTESIAN_POINT('Ctrl Pts',(104.46175523312,1.68188930259684,339.623768195784));
#36664=CARTESIAN_POINT('Ctrl Pts',(104.454006542562,1.81025835630819,339.575038532059));
#36665=CARTESIAN_POINT('Ctrl Pts',(104.446257852004,1.93639700970948,339.521012019812));
#36666=CARTESIAN_POINT('Ctrl Pts',(104.438510773626,2.06250941891041,339.466996748233));
#36667=CARTESIAN_POINT('Ctrl Pts',(104.430763695249,2.18639199175782,339.407686973991));
#36668=CARTESIAN_POINT('Ctrl Pts',(104.423016616871,2.30757731110058,339.343301741279));
#36669=CARTESIAN_POINT('Ctrl Pts',(104.415269473565,2.42876364609295,339.278915968956));
#36670=CARTESIAN_POINT('Ctrl Pts',(104.407522330259,2.54725233731143,339.209454836711));
#36671=CARTESIAN_POINT('Ctrl Pts',(104.399775186953,2.66260044727664,339.135183420438));
#36672=CARTESIAN_POINT('Ctrl Pts',(104.392026301925,2.77797448994597,339.060895306373));
#36673=CARTESIAN_POINT('Ctrl Pts',(104.384277416897,2.89020621778648,338.981794967874));
#36674=CARTESIAN_POINT('Ctrl Pts',(104.376528531869,2.99888190178801,338.898190657424));
#36675=CARTESIAN_POINT('Ctrl Pts',(104.368771422094,3.10767293528331,338.814497608495));
#36676=CARTESIAN_POINT('Ctrl Pts',(104.36101431232,3.2129000748831,338.726291276704));
#36677=CARTESIAN_POINT('Ctrl Pts',(104.353257202545,3.31418249364234,338.633920398321));
#36678=CARTESIAN_POINT('Ctrl Pts',(104.345495947619,3.41551903448778,338.541500159894));
#36679=CARTESIAN_POINT('Ctrl Pts',(104.337734692692,3.51290637686259,338.444911215676));
#36680=CARTESIAN_POINT('Ctrl Pts',(104.329973437766,3.60600150984952,338.344538260128));
#36681=CARTESIAN_POINT('Ctrl Pts',(104.322199767362,3.6992455647096,338.244004740564));
#36682=CARTESIAN_POINT('Ctrl Pts',(104.314426096957,3.78818343589915,338.13967541123));
#36683=CARTESIAN_POINT('Ctrl Pts',(104.306652426552,3.87251271086054,338.031967738404));
#36684=CARTESIAN_POINT('Ctrl Pts',(104.299240622375,3.95291643778421,337.929273883661));
#36685=CARTESIAN_POINT('Ctrl Pts',(104.291828818198,4.02913080480014,337.823509364534));
#36686=CARTESIAN_POINT('Ctrl Pts',(104.284417014021,4.10093198987428,337.715057987765));
#36687=CARTESIAN_POINT('Ctrl Pts',(104.276641935242,4.17625236491337,337.60129108596));
#36688=CARTESIAN_POINT('Ctrl Pts',(104.268866856464,4.24695403946529,337.484207760679));
#36689=CARTESIAN_POINT('Ctrl Pts',(104.261091777686,4.31273097402997,337.364219661568));
#36690=CARTESIAN_POINT('Ctrl Pts',(104.253326266637,4.37842696588925,337.24437921545));
#36691=CARTESIAN_POINT('Ctrl Pts',(104.245560755588,4.4392100897353,337.121641447226));
#36692=CARTESIAN_POINT('Ctrl Pts',(104.237795244539,4.49481695895252,336.996447737361));
#36693=CARTESIAN_POINT('Ctrl Pts',(104.230037433016,4.55036869379697,336.871378157424));
#36694=CARTESIAN_POINT('Ctrl Pts',(104.222279621494,4.60075422987901,336.743857836701));
#36695=CARTESIAN_POINT('Ctrl Pts',(104.214521809972,4.64575576647428,336.614353251544));
#36696=CARTESIAN_POINT('Ctrl Pts',(104.206769836449,4.69072343798624,336.484946122694));
#36697=CARTESIAN_POINT('Ctrl Pts',(104.199017862926,4.73031504680062,336.353558069327));
#36698=CARTESIAN_POINT('Ctrl Pts',(104.191265889403,4.76436079661151,336.220675739995));
#36699=CARTESIAN_POINT('Ctrl Pts',(104.183517198845,4.79839212802707,336.087849686408));
#36700=CARTESIAN_POINT('Ctrl Pts',(104.175768508288,4.82688217497702,335.953530993359));
#36701=CARTESIAN_POINT('Ctrl Pts',(104.16801981773,4.84971099141352,335.818221462847));
#36702=CARTESIAN_POINT('Ctrl Pts',(104.160272739352,4.87253505812408,335.682940084612));
#36703=CARTESIAN_POINT('Ctrl Pts',(104.152525660974,4.88970017219383,335.54666866415));
#36704=CARTESIAN_POINT('Ctrl Pts',(104.144778582596,4.90113758631536,335.409918799894));
#36705=CARTESIAN_POINT('Ctrl Pts',(104.137031439291,4.91257509629344,335.273167789543));
#36706=CARTESIAN_POINT('Ctrl Pts',(104.129284295985,4.91828477799844,335.135938716916));
#36707=CARTESIAN_POINT('Ctrl Pts',(104.121537152679,4.91824984051819,334.998747505363));
#36708=CARTESIAN_POINT('Ctrl Pts',(104.113788267651,4.91821489518325,334.861525450314));
#36709=CARTESIAN_POINT('Ctrl Pts',(104.106039382623,4.91243276079728,334.724341664076));
#36710=CARTESIAN_POINT('Ctrl Pts',(104.098290497595,4.90093876094261,334.587710873306));
#36711=CARTESIAN_POINT('Ctrl Pts',(104.09053338782,4.88943256123775,334.450935061203));
#36712=CARTESIAN_POINT('Ctrl Pts',(104.082776278045,4.8722024182041,334.314713807181));
#36713=CARTESIAN_POINT('Ctrl Pts',(104.07501916827,4.84933550430027,334.179556077947));
#36714=CARTESIAN_POINT('Ctrl Pts',(104.067257913344,4.82645637104883,334.044326124746));
#36715=CARTESIAN_POINT('Ctrl Pts',(104.059496658418,4.79793454626403,333.910161210886));
#36716=CARTESIAN_POINT('Ctrl Pts',(104.051735403492,4.76390790483787,333.777557961814));
#36717=CARTESIAN_POINT('Ctrl Pts',(104.043961733087,4.72982683187461,333.644742590759));
#36718=CARTESIAN_POINT('Ctrl Pts',(104.036188062683,4.69022345842358,333.513494250952));
#36719=CARTESIAN_POINT('Ctrl Pts',(104.028414392278,4.64528518799639,333.384293162519));
#36720=CARTESIAN_POINT('Ctrl Pts',(104.021002588101,4.60243880486978,333.26110641584));
#36721=CARTESIAN_POINT('Ctrl Pts',(104.013590783924,4.55474313152118,333.139780878589));
#36722=CARTESIAN_POINT('Ctrl Pts',(104.006178979747,4.50239979628299,333.020712467343));
#36723=CARTESIAN_POINT('Ctrl Pts',(103.998403900969,4.44749095826124,332.895808158573));
#36724=CARTESIAN_POINT('Ctrl Pts',(103.99062882219,4.38729382513031,332.772993106539));
#36725=CARTESIAN_POINT('Ctrl Pts',(103.982853743412,4.32198894632623,332.652747433629));
#36726=CARTESIAN_POINT('Ctrl Pts',(103.975088232363,4.25676442933307,332.532649730675));
#36727=CARTESIAN_POINT('Ctrl Pts',(103.967322721314,4.1864448575858,332.415115456004));
#36728=CARTESIAN_POINT('Ctrl Pts',(103.959557210265,4.11125886372488,332.300604953338));
#36729=CARTESIAN_POINT('Ctrl Pts',(103.951799398742,4.03614741699566,332.186207988168));
#36730=CARTESIAN_POINT('Ctrl Pts',(103.94404158722,3.95617936346873,332.074829153291));
#36731=CARTESIAN_POINT('Ctrl Pts',(103.936283775698,3.87162910859075,331.966904039102));
#36732=CARTESIAN_POINT('Ctrl Pts',(103.928531802175,3.7871424804607,331.859060141985));
#36733=CARTESIAN_POINT('Ctrl Pts',(103.920779828652,3.69808075463874,331.754665098761));
#36734=CARTESIAN_POINT('Ctrl Pts',(103.913027855129,3.60476127775036,331.654125048223));
#36735=CARTESIAN_POINT('Ctrl Pts',(103.905279164571,3.51148132171605,331.553627576455));
#36736=CARTESIAN_POINT('Ctrl Pts',(103.897530474014,3.41394746633127,331.456982136153));
#36737=CARTESIAN_POINT('Ctrl Pts',(103.889781783456,3.31251677791223,331.364561146361));
#36738=CARTESIAN_POINT('Ctrl Pts',(103.882034705078,3.21110719299501,331.272159385527));
#36739=CARTESIAN_POINT('Ctrl Pts',(103.874287626701,3.10580267646215,331.183980590039));
#36740=CARTESIAN_POINT('Ctrl Pts',(103.866540548323,2.99699623923926,331.100359426244));
#36741=CARTESIAN_POINT('Ctrl Pts',(103.858793405017,2.88818889011371,331.016737561622));
#36742=CARTESIAN_POINT('Ctrl Pts',(103.851046261711,2.77587987167948,330.937673643065));
#36743=CARTESIAN_POINT('Ctrl Pts',(103.843299118405,2.6604939483639,330.863460986136));
#36744=CARTESIAN_POINT('Ctrl Pts',(103.835550233377,2.54508208384367,330.789231644627));
#36745=CARTESIAN_POINT('Ctrl Pts',(103.827801348349,2.42659226661401,330.719855946451));
#36746=CARTESIAN_POINT('Ctrl Pts',(103.820052463321,2.30547645691958,330.655582735384));
#36747=CARTESIAN_POINT('Ctrl Pts',(103.812295353546,2.18423209365288,330.591241304067));
#36748=CARTESIAN_POINT('Ctrl Pts',(103.804538243772,2.06035651593169,330.532013362007));
#36749=CARTESIAN_POINT('Ctrl Pts',(103.796781133997,1.93432489873964,330.478101035116));
#36750=CARTESIAN_POINT('Ctrl Pts',(103.789019879071,1.80822593428116,330.424159899202));
#36751=CARTESIAN_POINT('Ctrl Pts',(103.781258624145,1.67996899996075,330.375540176879));
#36752=CARTESIAN_POINT('Ctrl Pts',(103.773497369218,1.55004633072628,330.332394678735));
#36753=CARTESIAN_POINT('Ctrl Pts',(103.765723698814,1.41991582756264,330.289180161855));
#36754=CARTESIAN_POINT('Ctrl Pts',(103.757950028409,1.2881146407426,330.251457475793));
#36755=CARTESIAN_POINT('Ctrl Pts',(103.750176358004,1.15514801241047,330.219328903603));
#36756=CARTESIAN_POINT('Ctrl Pts',(103.742764553827,1.02837101261596,330.188695924179));
#36757=CARTESIAN_POINT('Ctrl Pts',(103.73535274965,0.900534914346303,330.163148023575));
#36758=CARTESIAN_POINT('Ctrl Pts',(103.727940945473,0.772081764955789,330.142729901403));
#36759=CARTESIAN_POINT('Ctrl Pts',(103.720165866695,0.637332744072424,330.121311026241));
#36760=CARTESIAN_POINT('Ctrl Pts',(103.712390787916,0.501478823824455,330.105469807959));
#36761=CARTESIAN_POINT('Ctrl Pts',(103.704615709138,0.365021455031457,330.095314240457));
#36762=CARTESIAN_POINT('Ctrl Pts',(103.696850198089,0.228732005718524,330.085171170027));
#36763=CARTESIAN_POINT('Ctrl Pts',(103.68908468704,0.0918409714555158,330.080699857972));
#36764=CARTESIAN_POINT('Ctrl Pts',(103.681319175991,-0.045140808660564,
330.081957160628));
#36765=CARTESIAN_POINT('Ctrl Pts',(103.673561364469,-0.181986770943126,
330.083213216666));
#36766=CARTESIAN_POINT('Ctrl Pts',(103.665803552946,-0.318922911683839,
330.090186580452));
#36767=CARTESIAN_POINT('Ctrl Pts',(103.658045741424,-0.455434437093222,
330.10288222155));
#36768=CARTESIAN_POINT('Ctrl Pts',(103.650293767901,-0.591843233250147,
330.115568308776));
#36769=CARTESIAN_POINT('Ctrl Pts',(103.642541794378,-0.727827662469809,
330.133968065993));
#36770=CARTESIAN_POINT('Ctrl Pts',(103.634789820855,-0.862874459509467,
330.158034414659));
#36771=CARTESIAN_POINT('Ctrl Pts',(103.627041130298,-0.997864064151229,
330.182090571212));
#36772=CARTESIAN_POINT('Ctrl Pts',(103.61929243974,-1.13191644238182,330.211808477737));
#36773=CARTESIAN_POINT('Ctrl Pts',(103.611543749183,-1.26452519000914,330.247089406865));
#36774=CARTESIAN_POINT('Ctrl Pts',(103.603796670805,-1.39710634727831,330.282362995502));
#36775=CARTESIAN_POINT('Ctrl Pts',(103.596049592427,-1.5282440938834,330.323197204091));
#36776=CARTESIAN_POINT('Ctrl Pts',(103.588302514049,-1.65744432099134,330.369442648523));
#36777=CARTESIAN_POINT('Ctrl Pts',(103.580555370743,-1.78664563092163,330.415688480538));
#36778=CARTESIAN_POINT('Ctrl Pts',(103.572808227438,-1.9139090209562,330.467345507128));
#36779=CARTESIAN_POINT('Ctrl Pts',(103.565061084132,-2.03875797137367,330.524215264709));
#36780=CARTESIAN_POINT('Ctrl Pts',(103.557312199104,-2.16363499048649,330.58109780782));
#36781=CARTESIAN_POINT('Ctrl Pts',(103.549563314076,-2.28609613419626,330.643195251938));
#36782=CARTESIAN_POINT('Ctrl Pts',(103.541814429047,-2.40568756284156,330.710262197699));
#36783=CARTESIAN_POINT('Ctrl Pts',(103.534057319273,-2.52540592706458,330.777400329009));
#36784=CARTESIAN_POINT('Ctrl Pts',(103.526300209498,-2.6422481501996,330.849518307137));
#36785=CARTESIAN_POINT('Ctrl Pts',(103.518543099723,-2.75578711580683,330.926325929231));
#36786=CARTESIAN_POINT('Ctrl Pts',(103.510781844797,-2.86938675300669,331.003174594863));
#36787=CARTESIAN_POINT('Ctrl Pts',(103.503020589871,-2.97967930130635,331.084717665626));
#36788=CARTESIAN_POINT('Ctrl Pts',(103.495259334945,-3.08626988244834,331.17062390523));
#36789=CARTESIAN_POINT('Ctrl Pts',(103.48748566454,-3.19303097378257,331.256667566821));
#36790=CARTESIAN_POINT('Ctrl Pts',(103.479711994135,-3.29607797020962,331.347088086718));
#36791=CARTESIAN_POINT('Ctrl Pts',(103.471938323731,-3.39505144421095,331.441515947252));
#36792=CARTESIAN_POINT('Ctrl Pts',(103.464526519554,-3.48941767918654,331.531548168161));
#36793=CARTESIAN_POINT('Ctrl Pts',(103.457114715376,-3.58008090185183,331.625222835505));
#36794=CARTESIAN_POINT('Ctrl Pts',(103.449702911199,-3.66676430616309,331.722192411756));
#36795=CARTESIAN_POINT('Ctrl Pts',(103.442001504964,-3.75683469853705,331.822950888545));
#36796=CARTESIAN_POINT('Ctrl Pts',(103.434300098729,-3.8429057633272,331.927600371559));
#36797=CARTESIAN_POINT('Ctrl Pts',(103.426598692494,-3.92461757230766,332.035786786745));
#36798=CARTESIAN_POINT('Ctrl Pts',(103.418909461983,-4.00620019703642,332.143802162014));
#36799=CARTESIAN_POINT('Ctrl Pts',(103.411220231472,-4.0834370496851,332.255343020752));
#36800=CARTESIAN_POINT('Ctrl Pts',(103.40353100096,-4.15600610259396,332.370019707735));
#36801=CARTESIAN_POINT('Ctrl Pts',(103.395848776324,-4.22850903578516,332.484591909544));
#36802=CARTESIAN_POINT('Ctrl Pts',(103.388166551688,-4.29635241396984,332.602293923805));
#36803=CARTESIAN_POINT('Ctrl Pts',(103.380484327052,-4.35925535044355,332.722704267749));
#36804=CARTESIAN_POINT('Ctrl Pts',(103.372807360204,-4.42211523555385,332.843032201717));
#36805=CARTESIAN_POINT('Ctrl Pts',(103.365130393355,-4.48004121993017,332.966064426588));
#36806=CARTESIAN_POINT('Ctrl Pts',(103.357453426506,-4.53279679509627,333.091352238661));
#36807=CARTESIAN_POINT('Ctrl Pts',(103.349779973757,-4.58552822161464,333.216582700753));
#36808=CARTESIAN_POINT('Ctrl Pts',(103.342106521008,-4.63309379327532,333.344066328791));
#36809=CARTESIAN_POINT('Ctrl Pts',(103.334433068259,-4.67530408647686,333.473332137801));
#36810=CARTESIAN_POINT('Ctrl Pts',(103.326759581296,-4.71751456788961,333.602598523193));
#36811=CARTESIAN_POINT('Ctrl Pts',(103.319086094332,-4.75436958686064,333.733646730297));
#36812=CARTESIAN_POINT('Ctrl Pts',(103.311412607368,-4.78572885309172,333.86598835668));
#36813=CARTESIAN_POINT('Ctrl Pts',(103.303739372935,-4.81708708730259,333.998325627756));
#36814=CARTESIAN_POINT('Ctrl Pts',(103.296066138502,-4.84294984225035,334.131955843638));
#36815=CARTESIAN_POINT('Ctrl Pts',(103.28839290407,-4.86322765882695,334.266378980045));
#36816=CARTESIAN_POINT('Ctrl Pts',(103.280714799051,-4.88351834674777,334.400887441538));
#36817=CARTESIAN_POINT('Ctrl Pts',(103.273036694033,-4.89821695898867,334.536189433322));
#36818=CARTESIAN_POINT('Ctrl Pts',(103.265358589015,-4.90728575814236,334.671778199333));
#36819=CARTESIAN_POINT('Ctrl Pts',(103.259084475506,-4.9146962683057,334.782573676389));
#36820=CARTESIAN_POINT('Ctrl Pts',(103.252810361998,-4.9183485878029,334.893560437054));
#36821=CARTESIAN_POINT('Ctrl Pts',(103.24653624849,-4.91824797603409,335.004461920724));
#36822=CARTESIAN_POINT('',(106.746536248459,-4.91824852393639,334.996189580397));
#36823=CARTESIAN_POINT('Ctrl Pts',(106.746536248459,-4.91824852393639,334.996189580397));
#36824=CARTESIAN_POINT('Ctrl Pts',(106.738885073854,-4.9183528630231,335.130863871606));
#36825=CARTESIAN_POINT('Ctrl Pts',(106.731233899249,-4.91292145302669,335.265744929164));
#36826=CARTESIAN_POINT('Ctrl Pts',(106.723582724644,-4.90192995717744,335.400332058954));
#36827=CARTESIAN_POINT('Ctrl Pts',(106.715939142596,-4.89094936861568,335.534785632717));
#36828=CARTESIAN_POINT('Ctrl Pts',(106.708295560548,-4.87441970043182,335.668945459565));
#36829=CARTESIAN_POINT('Ctrl Pts',(106.7006519785,-4.852368651929,335.802310119765));
#36830=CARTESIAN_POINT('Ctrl Pts',(106.692721533071,-4.82949002830698,335.94067995124));
#36831=CARTESIAN_POINT('Ctrl Pts',(106.684791087643,-4.80066747843367,336.078193324683));
#36832=CARTESIAN_POINT('Ctrl Pts',(106.676860642214,-4.76599113994609,336.214294658003));
#36833=CARTESIAN_POINT('Ctrl Pts',(106.66922570775,-4.73260694051098,336.345324468332));
#36834=CARTESIAN_POINT('Ctrl Pts',(106.661590773286,-4.69379749282756,336.47504515645));
#36835=CARTESIAN_POINT('Ctrl Pts',(106.653955838822,-4.64969532675885,336.602971126008));
#36836=CARTESIAN_POINT('Ctrl Pts',(106.646322084699,-4.60559997876458,336.730877318562));
#36837=CARTESIAN_POINT('Ctrl Pts',(106.638688330575,-4.5562136706169,336.856988962874));
#36838=CARTESIAN_POINT('Ctrl Pts',(106.631054576451,-4.50171850167197,336.980836589475));
#36839=CARTESIAN_POINT('Ctrl Pts',(106.623420236805,-4.447219152853,337.104693715404));
#36840=CARTESIAN_POINT('Ctrl Pts',(106.615785897159,-4.38761032693191,337.226286109175));
#36841=CARTESIAN_POINT('Ctrl Pts',(106.608151557513,-4.3231216381909,337.345165743376));
#36842=CARTESIAN_POINT('Ctrl Pts',(106.600514866197,-4.25861308445501,337.464081997075));
#36843=CARTESIAN_POINT('Ctrl Pts',(106.59287817488,-4.18922187160373,337.580283475428));
#36844=CARTESIAN_POINT('Ctrl Pts',(106.585241483564,-4.11522249065059,337.693348643407));
#36845=CARTESIAN_POINT('Ctrl Pts',(106.577596621492,-4.04114393523625,337.806534783665));
#36846=CARTESIAN_POINT('Ctrl Pts',(106.569951759419,-3.96244759290779,337.916577578988));
#36847=CARTESIAN_POINT('Ctrl Pts',(106.562306897347,-3.87945015744457,338.023086095103));
#36848=CARTESIAN_POINT('Ctrl Pts',(106.554657172124,-3.79639992455868,338.129662364818));
#36849=CARTESIAN_POINT('Ctrl Pts',(106.547007446901,-3.70904341289482,338.232699573942));
#36850=CARTESIAN_POINT('Ctrl Pts',(106.539357721678,-3.61773524267658,338.331842549761));
#36851=CARTESIAN_POINT('Ctrl Pts',(106.5316973497,-3.52629999133566,338.431123511048));
#36852=CARTESIAN_POINT('Ctrl Pts',(106.524036977723,-3.43090239176658,338.526499141421));
#36853=CARTESIAN_POINT('Ctrl Pts',(106.516376605745,-3.33193141217521,338.617653400626));
#36854=CARTESIAN_POINT('Ctrl Pts',(106.514358166568,-3.30585344843455,338.641671728788));
#36855=CARTESIAN_POINT('Ctrl Pts',(106.51233972739,-3.27952755584444,338.665397207074));
#36856=CARTESIAN_POINT('Ctrl Pts',(106.510321288212,-3.25296118483706,338.688824554305));
#36857=CARTESIAN_POINT('Ctrl Pts',(106.502546209434,-3.15062685159784,338.779067288543));
#36858=CARTESIAN_POINT('Ctrl Pts',(106.494771130655,-3.04437273219843,338.865191001619));
#36859=CARTESIAN_POINT('Ctrl Pts',(106.486996051877,-2.93456450411663,338.946835977549));
#36860=CARTESIAN_POINT('Ctrl Pts',(106.479230540828,-2.82489140205007,339.028380484139));
#36861=CARTESIAN_POINT('Ctrl Pts',(106.471465029779,-2.7116732040988,339.105456988639));
#36862=CARTESIAN_POINT('Ctrl Pts',(106.46369951873,-2.59531089901102,339.177743936621));
#36863=CARTESIAN_POINT('Ctrl Pts',(106.455941707208,-2.47906396748767,339.249959211884));
#36864=CARTESIAN_POINT('Ctrl Pts',(106.448183895685,-2.35967946249722,339.317394176195));
#36865=CARTESIAN_POINT('Ctrl Pts',(106.440426084163,-2.23758949625525,339.379768978924));
#36866=CARTESIAN_POINT('Ctrl Pts',(106.43267411064,-2.11559140658456,339.442096842637));
#36867=CARTESIAN_POINT('Ctrl Pts',(106.424922137117,-1.99089225478948,339.499371947155));
#36868=CARTESIAN_POINT('Ctrl Pts',(106.417170163594,-1.86395073202679,339.551359217978));
#36869=CARTESIAN_POINT('Ctrl Pts',(106.409421473037,-1.73706296907437,339.603324472161));
#36870=CARTESIAN_POINT('Ctrl Pts',(106.401672782479,-1.60793508489533,339.650006198831));
#36871=CARTESIAN_POINT('Ctrl Pts',(106.393924091921,-1.47704763217791,339.691216617763));
#36872=CARTESIAN_POINT('Ctrl Pts',(106.386177013543,-1.34618741168822,339.732418462523));
#36873=CARTESIAN_POINT('Ctrl Pts',(106.378429935166,-1.21356872344179,339.768151146493));
#36874=CARTESIAN_POINT('Ctrl Pts',(106.370682856788,-1.07968886084365,339.798276255727));
#36875=CARTESIAN_POINT('Ctrl Pts',(106.362935713482,-0.945807876203221,
339.828401617438));
#36876=CARTESIAN_POINT('Ctrl Pts',(106.355188570176,-0.810666077468183,
339.852919224868));
#36877=CARTESIAN_POINT('Ctrl Pts',(106.34744142687,-0.674772183311245,339.871741532874));
#36878=CARTESIAN_POINT('Ctrl Pts',(106.339692541842,-0.538847737321976,
339.890568072535));
#36879=CARTESIAN_POINT('Ctrl Pts',(106.331943656814,-0.402171246548947,
339.903696711254));
#36880=CARTESIAN_POINT('Ctrl Pts',(106.324194771786,-0.265257407458893,
339.911091688239));
#36881=CARTESIAN_POINT('Ctrl Pts',(106.316437662011,-0.12819824660535,339.918494514328));
#36882=CARTESIAN_POINT('Ctrl Pts',(106.308680552237,0.00909837488508905,
339.920151500675));
#36883=CARTESIAN_POINT('Ctrl Pts',(106.300923442462,0.146116339203136,339.916079034954));
#36884=CARTESIAN_POINT('Ctrl Pts',(106.293162187536,0.283207521540329,339.912004393038));
#36885=CARTESIAN_POINT('Ctrl Pts',(106.285400932609,0.420019360322044,339.90219422641));
#36886=CARTESIAN_POINT('Ctrl Pts',(106.277639677683,0.556040992825429,339.886716840251));
#36887=CARTESIAN_POINT('Ctrl Pts',(106.269866007279,0.69228021561138,339.871214695319));
#36888=CARTESIAN_POINT('Ctrl Pts',(106.262092336874,0.827726319746574,339.850027275336));
#36889=CARTESIAN_POINT('Ctrl Pts',(106.254318666469,0.961877884416177,339.82327419892));
#36890=CARTESIAN_POINT('Ctrl Pts',(106.246906862292,1.08978466147432,339.797766484649));
#36891=CARTESIAN_POINT('Ctrl Pts',(106.239495058115,1.21651442865383,339.767199683114));
#36892=CARTESIAN_POINT('Ctrl Pts',(106.232083253938,1.34164731334559,339.731719090256));
#36893=CARTESIAN_POINT('Ctrl Pts',(106.22430817516,1.47291333346866,339.694499487851));
#36894=CARTESIAN_POINT('Ctrl Pts',(106.216533096381,1.60283680203027,339.651754614939));
#36895=CARTESIAN_POINT('Ctrl Pts',(106.208758017603,1.73091733711911,339.603597314553));
#36896=CARTESIAN_POINT('Ctrl Pts',(106.200992506554,1.8588402609556,339.555499274791));
#36897=CARTESIAN_POINT('Ctrl Pts',(106.193226995505,1.98492440131458,339.502002195963));
#36898=CARTESIAN_POINT('Ctrl Pts',(106.185461484456,2.10868235819741,339.443269266512));
#36899=CARTESIAN_POINT('Ctrl Pts',(106.177703672934,2.23231760870585,339.38459457093));
#36900=CARTESIAN_POINT('Ctrl Pts',(106.169945861412,2.35363091478896,339.320694522333));
#36901=CARTESIAN_POINT('Ctrl Pts',(106.16218804989,2.47215310336668,339.251781049868));
#36902=CARTESIAN_POINT('Ctrl Pts',(106.154436076367,2.59058610023871,339.182919436976));
#36903=CARTESIAN_POINT('Ctrl Pts',(106.146684102844,2.70623182381113,339.109052105391));
#36904=CARTESIAN_POINT('Ctrl Pts',(106.138932129321,2.81864437081585,339.030437565993));
#36905=CARTESIAN_POINT('Ctrl Pts',(106.131183438763,2.93100931104025,338.951856319899));
#36906=CARTESIAN_POINT('Ctrl Pts',(106.123434748205,3.04014347839367,338.868532088168));
#36907=CARTESIAN_POINT('Ctrl Pts',(106.115686057648,3.14562890984503,338.780767359154));
#36908=CARTESIAN_POINT('Ctrl Pts',(106.10793897927,3.25109239417135,338.693020890325));
#36909=CARTESIAN_POINT('Ctrl Pts',(106.100191900892,3.35290835231354,338.60083601172));
#36910=CARTESIAN_POINT('Ctrl Pts',(106.092444822514,3.45069127503616,338.504556004245));
#36911=CARTESIAN_POINT('Ctrl Pts',(106.084697679209,3.54847501727372,338.408275189851));
#36912=CARTESIAN_POINT('Ctrl Pts',(106.076950535903,3.64222537815163,338.307899452371));
#36913=CARTESIAN_POINT('Ctrl Pts',(106.069203392597,3.73159344222866,338.203809208492));
#36914=CARTESIAN_POINT('Ctrl Pts',(106.061454507569,3.82098159814384,338.099695562916));
#36915=CARTESIAN_POINT('Ctrl Pts',(106.053705622541,3.9059852421832,337.991866045692));
#36916=CARTESIAN_POINT('Ctrl Pts',(106.045956737513,3.98629577054028,337.880734123843));
#36917=CARTESIAN_POINT('Ctrl Pts',(106.038199627738,4.06669154132203,337.769484245423));
#36918=CARTESIAN_POINT('Ctrl Pts',(106.030442517963,4.14238401645871,337.654925277707));
#36919=CARTESIAN_POINT('Ctrl Pts',(106.022685408189,4.21310767573346,337.537500103483));
#36920=CARTESIAN_POINT('Ctrl Pts',(106.014924153263,4.28386912747032,337.420012181));
#36921=CARTESIAN_POINT('Ctrl Pts',(106.007162898336,4.34965628528845,337.299655342946));
#36922=CARTESIAN_POINT('Ctrl Pts',(105.99940164341,4.41025013133962,337.176896148538));
#36923=CARTESIAN_POINT('Ctrl Pts',(105.991627973006,4.47094090779707,337.053940579425));
#36924=CARTESIAN_POINT('Ctrl Pts',(105.983854302601,4.52642161316247,336.928575332155));
#36925=CARTESIAN_POINT('Ctrl Pts',(105.976080632196,4.57652148971107,336.801286794687));
#36926=CARTESIAN_POINT('Ctrl Pts',(105.968668828019,4.62428920495381,336.679923569259));
#36927=CARTESIAN_POINT('Ctrl Pts',(105.961257023842,4.66716567820311,336.556812354141));
#36928=CARTESIAN_POINT('Ctrl Pts',(105.953845219665,4.70504587475491,336.432384857136));
#36929=CARTESIAN_POINT('Ctrl Pts',(105.946070140886,4.74478269257842,336.301858797854));
#36930=CARTESIAN_POINT('Ctrl Pts',(105.938295062108,4.77914666087071,336.169471677912));
#36931=CARTESIAN_POINT('Ctrl Pts',(105.930519983329,4.80796188638133,336.035705344972));
#36932=CARTESIAN_POINT('Ctrl Pts',(105.92275447228,4.83674165292247,335.902103620022));
#36933=CARTESIAN_POINT('Ctrl Pts',(105.914988961231,4.85998618108075,335.767126437491));
#36934=CARTESIAN_POINT('Ctrl Pts',(105.907223450182,4.87756893939187,335.631271973067));
#36935=CARTESIAN_POINT('Ctrl Pts',(105.89946563866,4.89513426434692,335.49555220874));
#36936=CARTESIAN_POINT('Ctrl Pts',(105.891707827138,4.90704894111149,335.358957278669));
#36937=CARTESIAN_POINT('Ctrl Pts',(105.883950015616,4.91323728895161,335.221996407528));
#36938=CARTESIAN_POINT('Ctrl Pts',(105.876198042093,4.91942097986372,335.085138603787));
#36939=CARTESIAN_POINT('Ctrl Pts',(105.86844606857,4.91988690161919,334.947915796015));
#36940=CARTESIAN_POINT('Ctrl Pts',(105.860694095047,4.91461113768627,334.810842848853));
#36941=CARTESIAN_POINT('Ctrl Pts',(105.852945404489,4.90933760804249,334.673827952165));
#36942=CARTESIAN_POINT('Ctrl Pts',(105.845196713932,4.89832724400769,334.536963179629));
#36943=CARTESIAN_POINT('Ctrl Pts',(105.837448023374,4.88160823071242,334.40076369908));
#36944=CARTESIAN_POINT('Ctrl Pts',(105.829700944996,4.8648926959475,334.26459255597));
#36945=CARTESIAN_POINT('Ctrl Pts',(105.821953866618,4.84247092199935,334.129086817239));
#36946=CARTESIAN_POINT('Ctrl Pts',(105.81420678824,4.81442295993736,333.994756434824));
#36947=CARTESIAN_POINT('Ctrl Pts',(105.806459644935,4.78637476280644,333.860424926591));
#36948=CARTESIAN_POINT('Ctrl Pts',(105.798712501629,4.75270036340273,333.727269176943));
#36949=CARTESIAN_POINT('Ctrl Pts',(105.790965358323,4.7135308440669,333.595788461616));
#36950=CARTESIAN_POINT('Ctrl Pts',(105.783216473295,4.67435251859141,333.464278186633));
#36951=CARTESIAN_POINT('Ctrl Pts',(105.775467588267,4.6296767264136,333.33444406986));
#36952=CARTESIAN_POINT('Ctrl Pts',(105.767718703239,4.57968415754549,333.206769373553));
#36953=CARTESIAN_POINT('Ctrl Pts',(105.759961593464,4.52963852604845,333.078959162005));
#36954=CARTESIAN_POINT('Ctrl Pts',(105.752204483689,4.47426498761729,332.953313314011));
#36955=CARTESIAN_POINT('Ctrl Pts',(105.744447373914,4.41379228361154,332.830294780476));
#36956=CARTESIAN_POINT('Ctrl Pts',(105.736686118988,4.35328726492628,332.707210509769));
#36957=CARTESIAN_POINT('Ctrl Pts',(105.728924864062,4.28767783806774,332.586756694108));
#36958=CARTESIAN_POINT('Ctrl Pts',(105.721163609136,4.21723781950897,332.469369992234));
#36959=CARTESIAN_POINT('Ctrl Pts',(105.713389938731,4.14668511987695,332.351795509895));
#36960=CARTESIAN_POINT('Ctrl Pts',(105.705616268327,4.07128660205224,332.23729827237));
#36961=CARTESIAN_POINT('Ctrl Pts',(105.697842597922,3.99135887324377,332.126285085907));
#36962=CARTESIAN_POINT('Ctrl Pts',(105.690430793745,3.91515179944236,332.020439589985));
#36963=CARTESIAN_POINT('Ctrl Pts',(105.683018989568,3.83482787211581,331.917761306283));
#36964=CARTESIAN_POINT('Ctrl Pts',(105.675607185391,3.75069328326275,331.81857218259));
#36965=CARTESIAN_POINT('Ctrl Pts',(105.667832106613,3.66243500758424,331.714521504474));
#36966=CARTESIAN_POINT('Ctrl Pts',(105.660057027834,3.56970416911645,331.613981843442));
#36967=CARTESIAN_POINT('Ctrl Pts',(105.652281949056,3.47281077790956,331.5173618673));
#36968=CARTESIAN_POINT('Ctrl Pts',(105.644516438007,3.37603662018921,331.42086078819));
#36969=CARTESIAN_POINT('Ctrl Pts',(105.636750926958,3.27511037574467,331.328270070105));
#36970=CARTESIAN_POINT('Ctrl Pts',(105.628985415909,3.17038249770311,331.239965707502));
#36971=CARTESIAN_POINT('Ctrl Pts',(105.621227604386,3.06575845765769,331.151748898932));
#36972=CARTESIAN_POINT('Ctrl Pts',(105.613469792864,2.95734058209763,331.067810238576));
#36973=CARTESIAN_POINT('Ctrl Pts',(105.605711981342,2.84551613372756,330.988488938667));
#36974=CARTESIAN_POINT('Ctrl Pts',(105.597960007819,2.73377583680112,330.909227330552));
#36975=CARTESIAN_POINT('Ctrl Pts',(105.590208034296,2.61863438722192,330.83457639188));
#36976=CARTESIAN_POINT('Ctrl Pts',(105.582456060773,2.5005118030427,330.76483485737));
#36977=CARTESIAN_POINT('Ctrl Pts',(105.574707370216,2.38243924384793,330.695122858443));
#36978=CARTESIAN_POINT('Ctrl Pts',(105.566958679658,2.26138839698723,330.630316326737));
#36979=CARTESIAN_POINT('Ctrl Pts',(105.5592099891,2.1378077306745,330.570670347652));
#36980=CARTESIAN_POINT('Ctrl Pts',(105.551462910722,2.01425277635156,330.511036778411));
#36981=CARTESIAN_POINT('Ctrl Pts',(105.543715832345,1.88816940132079,330.456561795927));
#36982=CARTESIAN_POINT('Ctrl Pts',(105.535968753967,1.76002975527161,330.407454047801));
#36983=CARTESIAN_POINT('Ctrl Pts',(105.528221610661,1.63188903528895,330.358345888105));
#36984=CARTESIAN_POINT('Ctrl Pts',(105.520474467355,1.50169237490352,330.314605192366));
#36985=CARTESIAN_POINT('Ctrl Pts',(105.512727324049,1.36993056190864,330.276391917395));
#36986=CARTESIAN_POINT('Ctrl Pts',(105.504978439021,1.23813912606116,330.238170051269));
#36987=CARTESIAN_POINT('Ctrl Pts',(105.497229553993,1.10478221273518,330.205478187562));
#36988=CARTESIAN_POINT('Ctrl Pts',(105.489480668965,0.970363989204162,330.178425901124));
#36989=CARTESIAN_POINT('Ctrl Pts',(105.481723559191,0.835803092781339,330.151344901109));
#36990=CARTESIAN_POINT('Ctrl Pts',(105.473966449416,0.700179019689055,330.129915513011));
#36991=CARTESIAN_POINT('Ctrl Pts',(105.466209339641,0.564004860293756,330.11419591264));
#36992=CARTESIAN_POINT('Ctrl Pts',(105.458448084715,0.427757933781589,330.098467912217));
#36993=CARTESIAN_POINT('Ctrl Pts',(105.450686829789,0.290960724881314,330.088455807685));
#36994=CARTESIAN_POINT('Ctrl Pts',(105.442925574863,0.154128607051445,330.084165642031));
#36995=CARTESIAN_POINT('Ctrl Pts',(105.435151904458,0.017077602426625,330.079868613511));
#36996=CARTESIAN_POINT('Ctrl Pts',(105.427378234053,-0.120008031660257,
330.081311810631));
#36997=CARTESIAN_POINT('Ctrl Pts',(105.419604563649,-0.256614868829094,
330.088449137839));
#36998=CARTESIAN_POINT('Ctrl Pts',(105.412192759471,-0.38686262486442,330.095254220748));
#36999=CARTESIAN_POINT('Ctrl Pts',(105.404780955294,-0.516674870241541,
330.107235213883));
#37000=CARTESIAN_POINT('Ctrl Pts',(105.397369151117,-0.645615174136864,
330.124308858282));
#37001=CARTESIAN_POINT('Ctrl Pts',(105.389594072339,-0.780875226417314,
330.142219332853));
#37002=CARTESIAN_POINT('Ctrl Pts',(105.38181899356,-0.915603149888324,330.165790893697));
#37003=CARTESIAN_POINT('Ctrl Pts',(105.374043914782,-1.04928752284639,330.194984000349));
#37004=CARTESIAN_POINT('Ctrl Pts',(105.366278403733,-1.18280738867303,330.224141183026));
#37005=CARTESIAN_POINT('Ctrl Pts',(105.358512892684,-1.31528588086312,330.258906064736));
#37006=CARTESIAN_POINT('Ctrl Pts',(105.350747381635,-1.44621716736012,330.299187414145));
#37007=CARTESIAN_POINT('Ctrl Pts',(105.342989570112,-1.57701863510466,330.339428824478));
#37008=CARTESIAN_POINT('Ctrl Pts',(105.33523175859,-1.70627557883314,330.385175703513));
#37009=CARTESIAN_POINT('Ctrl Pts',(105.327473947068,-1.8334931776704,330.436285960981));
#37010=CARTESIAN_POINT('Ctrl Pts',(105.319721973545,-1.96061504122989,330.48735775636));
#37011=CARTESIAN_POINT('Ctrl Pts',(105.311970000022,-2.08570025334977,330.543784751361));
#37012=CARTESIAN_POINT('Ctrl Pts',(105.304218026499,-2.20827030576032,330.60537540634));
#37013=CARTESIAN_POINT('Ctrl Pts',(105.296469335941,-2.33078844968148,330.666939977642));
#37014=CARTESIAN_POINT('Ctrl Pts',(105.288720645384,-2.45079320391194,330.73366368437));
#37015=CARTESIAN_POINT('Ctrl Pts',(105.280971954826,-2.56782736981495,330.805307441382));
#37016=CARTESIAN_POINT('Ctrl Pts',(105.273224876448,-2.68483718578234,330.876936292311));
#37017=CARTESIAN_POINT('Ctrl Pts',(105.265477798071,-2.798877309618,330.95348295345));
#37018=CARTESIAN_POINT('Ctrl Pts',(105.257730719693,-2.90951677781358,331.034663295239));
#37019=CARTESIAN_POINT('Ctrl Pts',(105.249983576387,-3.02015717327394,331.115844317398));
#37020=CARTESIAN_POINT('Ctrl Pts',(105.242236433081,-3.12739654110512,331.201658866435));
#37021=CARTESIAN_POINT('Ctrl Pts',(105.234489289775,-3.23083477677504,331.291780790234));
#37022=CARTESIAN_POINT('Ctrl Pts',(105.226740404747,-3.33429626755688,331.381922975354));
#37023=CARTESIAN_POINT('Ctrl Pts',(105.218991519719,-3.43395463101785,331.476374205505));
#37024=CARTESIAN_POINT('Ctrl Pts',(105.211242634691,-3.5294448894884,331.574769812908));
#37025=CARTESIAN_POINT('Ctrl Pts',(105.203485524916,-3.62503650230577,331.673269858426));
#37026=CARTESIAN_POINT('Ctrl Pts',(105.195728415141,-3.71645089999087,331.775722363384));
#37027=CARTESIAN_POINT('Ctrl Pts',(105.187971305367,-3.80336149862639,331.881727341417));
#37028=CARTESIAN_POINT('Ctrl Pts',(105.18021005044,-3.8903185395069,331.98778896512));
#37029=CARTESIAN_POINT('Ctrl Pts',(105.172448795514,-3.97276675096495,332.097406532268));
#37030=CARTESIAN_POINT('Ctrl Pts',(105.164687540588,-4.05042215317255,332.210149924532));
#37031=CARTESIAN_POINT('Ctrl Pts',(105.156913870183,-4.12820177871589,332.32307366948));
#37032=CARTESIAN_POINT('Ctrl Pts',(105.149140199779,-4.20117306604447,332.43913290055));
#37033=CARTESIAN_POINT('Ctrl Pts',(105.141366529374,-4.26909693341785,332.557870921597));
#37034=CARTESIAN_POINT('Ctrl Pts',(105.133954725197,-4.33385892842347,332.671081659197));
#37035=CARTESIAN_POINT('Ctrl Pts',(105.12654292102,-4.39403271029031,332.78672714861));
#37036=CARTESIAN_POINT('Ctrl Pts',(105.119131116843,-4.44945211549495,332.904395329644));
#37037=CARTESIAN_POINT('Ctrl Pts',(105.110702461519,-4.51247470130265,333.03820681695));
#37038=CARTESIAN_POINT('Ctrl Pts',(105.102273806194,-4.56952356562858,333.175004286875));
#37039=CARTESIAN_POINT('Ctrl Pts',(105.09384515087,-4.62032959520875,333.314254617643));
#37040=CARTESIAN_POINT('Ctrl Pts',(105.085444938978,-4.67096417420701,333.453035032725));
#37041=CARTESIAN_POINT('Ctrl Pts',(105.077044727086,-4.7153978376093,333.594251532157));
#37042=CARTESIAN_POINT('Ctrl Pts',(105.068644515194,-4.753409471131,333.737351409828));
#37043=CARTESIAN_POINT('Ctrl Pts',(105.060261676269,-4.79134249058272,333.88015533432));
#37044=CARTESIAN_POINT('Ctrl Pts',(105.051878837344,-4.82287988160151,334.02483459894));
#37045=CARTESIAN_POINT('Ctrl Pts',(105.043495998419,-4.84784917077349,334.170818789449));
#37046=CARTESIAN_POINT('Ctrl Pts',(105.035140929155,-4.87273574468608,334.316319381081));
#37047=CARTESIAN_POINT('Ctrl Pts',(105.026785859891,-4.8910975567269,334.463115997978));
#37048=CARTESIAN_POINT('Ctrl Pts',(105.018430790627,-4.90281261842756,334.610626797163));
#37049=CARTESIAN_POINT('Ctrl Pts',(105.011132609926,-4.91304576366047,334.739477969274));
#37050=CARTESIAN_POINT('Ctrl Pts',(105.003834429225,-4.9182080748459,334.868873698525));
#37051=CARTESIAN_POINT('Ctrl Pts',(104.996536248525,-4.91824974554793,334.998417938773));
#37052=CARTESIAN_POINT('',(108.496536248524,-4.9182486817404,335.003600980256));
#37053=CARTESIAN_POINT('Ctrl Pts',(108.49653624849,-4.91824868173996,335.003600980854));
#37054=CARTESIAN_POINT('Ctrl Pts',(108.483686675037,-4.91808315126232,335.22968384175));
#37055=CARTESIAN_POINT('Ctrl Pts',(108.470837101584,-4.9023277300516,335.455205193581));
#37056=CARTESIAN_POINT('Ctrl Pts',(108.45798752813,-4.87121828787386,335.678539206224));
#37057=CARTESIAN_POINT('Ctrl Pts',(108.450212449352,-4.85239444406579,335.813675173851));
#37058=CARTESIAN_POINT('Ctrl Pts',(108.442437370574,-4.82791323807937,335.948240780144));
#37059=CARTESIAN_POINT('Ctrl Pts',(108.434662291795,-4.79781766449557,336.081724882192));
#37060=CARTESIAN_POINT('Ctrl Pts',(108.426896780746,-4.76775912543104,336.215044723556));
#37061=CARTESIAN_POINT('Ctrl Pts',(108.419131269697,-4.73210005052074,336.347285331047));
#37062=CARTESIAN_POINT('Ctrl Pts',(108.411365758648,-4.69093508627443,336.477941500486));
#37063=CARTESIAN_POINT('Ctrl Pts',(108.403607947126,-4.64981093720996,336.608468123953));
#37064=CARTESIAN_POINT('Ctrl Pts',(108.395850135604,-4.60319187943937,336.737413065289));
#37065=CARTESIAN_POINT('Ctrl Pts',(108.388092324081,-4.55122334285371,336.864282474831));
#37066=CARTESIAN_POINT('Ctrl Pts',(108.380340350558,-4.49929391423994,336.99105641112));
#37067=CARTESIAN_POINT('Ctrl Pts',(108.372588377035,-4.44202316724143,337.115757564259));
#37068=CARTESIAN_POINT('Ctrl Pts',(108.364836403512,-4.3796058697932,337.237908730885));
#37069=CARTESIAN_POINT('Ctrl Pts',(108.357087712955,-4.31721500610749,337.36000816642));
#37070=CARTESIAN_POINT('Ctrl Pts',(108.349339022397,-4.24968210446359,337.479559415987));
#37071=CARTESIAN_POINT('Ctrl Pts',(108.341590331839,-4.17724933325099,337.596106906573));
#37072=CARTESIAN_POINT('Ctrl Pts',(108.333843253462,-4.10483163228136,337.71263014848));
#37073=CARTESIAN_POINT('Ctrl Pts',(108.326096175084,-4.02751629571281,337.826150542714));
#37074=CARTESIAN_POINT('Ctrl Pts',(108.318349096706,-3.94559035808407,337.9362390551));
#37075=CARTESIAN_POINT('Ctrl Pts',(108.3106019534,-3.86366373383718,338.046328490133));
#37076=CARTESIAN_POINT('Ctrl Pts',(108.302854810094,-3.77712666481263,338.152985672376));
#37077=CARTESIAN_POINT('Ctrl Pts',(108.295107666788,-3.68630799867523,338.255812709817));
#37078=CARTESIAN_POINT('Ctrl Pts',(108.28735878176,-3.59546891457343,338.358662864958));
#37079=CARTESIAN_POINT('Ctrl Pts',(108.279609896732,-3.50034657660713,338.4576808689));
#37080=CARTESIAN_POINT('Ctrl Pts',(108.271861011704,-3.40130810991624,338.55250421589));
#37081=CARTESIAN_POINT('Ctrl Pts',(108.264103901929,-3.30216452277361,338.647428209361));
#37082=CARTESIAN_POINT('Ctrl Pts',(108.256346792155,-3.19909678644762,338.738148381346));
#37083=CARTESIAN_POINT('Ctrl Pts',(108.24858968238,-3.0925070844845,338.824340857574));
#37084=CARTESIAN_POINT('Ctrl Pts',(108.240828427454,-2.98586042439274,338.910579392306));
#37085=CARTESIAN_POINT('Ctrl Pts',(108.233067172527,-2.87568836235641,338.992285177577));
#37086=CARTESIAN_POINT('Ctrl Pts',(108.225305917601,-2.76242292537484,339.069177145795));
#37087=CARTESIAN_POINT('Ctrl Pts',(108.217532247197,-2.64897630060723,339.146192116104));
#37088=CARTESIAN_POINT('Ctrl Pts',(108.209758576792,-2.53242674501801,339.218377675484));
#37089=CARTESIAN_POINT('Ctrl Pts',(108.201984906387,-2.41323255949811,339.285497832957));
#37090=CARTESIAN_POINT('Ctrl Pts',(108.19457310221,-2.29958689199112,339.349493530951));
#37091=CARTESIAN_POINT('Ctrl Pts',(108.187161298033,-2.18353752487874,339.408884672028));
#37092=CARTESIAN_POINT('Ctrl Pts',(108.179749493856,-2.06549763150288,339.463507880217));
#37093=CARTESIAN_POINT('Ctrl Pts',(108.171974415078,-1.94167225132945,339.520808334552));
#37094=CARTESIAN_POINT('Ctrl Pts',(108.164199336299,-1.81526497687633,339.573042737093));
#37095=CARTESIAN_POINT('Ctrl Pts',(108.156424257521,-1.68672890595508,339.61997063414));
#37096=CARTESIAN_POINT('Ctrl Pts',(108.148658746472,-1.55835100685203,339.666840783422));
#37097=CARTESIAN_POINT('Ctrl Pts',(108.140893235423,-1.42784988723146,339.708417287256));
#37098=CARTESIAN_POINT('Ctrl Pts',(108.133127724374,-1.29570160272429,339.744506340938));
#37099=CARTESIAN_POINT('Ctrl Pts',(108.125369912851,-1.16368434362604,339.780559612218));
#37100=CARTESIAN_POINT('Ctrl Pts',(108.117612101329,-1.03002354437659,339.811136158581));
#37101=CARTESIAN_POINT('Ctrl Pts',(108.109854289807,-0.895213194151686,
339.836091024734));
#37102=CARTESIAN_POINT('Ctrl Pts',(108.102102316284,-0.760504292990412,
339.86102711156));
#37103=CARTESIAN_POINT('Ctrl Pts',(108.094350342761,-0.624647945537534,
339.880349867905));
#37104=CARTESIAN_POINT('Ctrl Pts',(108.086598369238,-0.488150842387499,
339.893964836161));
#37105=CARTESIAN_POINT('Ctrl Pts',(108.07884967868,-0.351711545841687,339.907574038469));
#37106=CARTESIAN_POINT('Ctrl Pts',(108.071100988123,-0.214632421450255,
339.915480221715));
#37107=CARTESIAN_POINT('Ctrl Pts',(108.063352297565,-0.0774276214902788,
339.917640493766));
#37108=CARTESIAN_POINT('Ctrl Pts',(108.055605219187,0.0597486318650154,
339.919800316355));
#37109=CARTESIAN_POINT('Ctrl Pts',(108.047858140809,0.197050118198452,339.916216599503));
#37110=CARTESIAN_POINT('Ctrl Pts',(108.040111062432,0.333960722659175,339.906898541668));
#37111=CARTESIAN_POINT('Ctrl Pts',(108.032363919126,0.470872474562539,339.897580405738));
#37112=CARTESIAN_POINT('Ctrl Pts',(108.02461677582,0.607392948086891,339.882527859507));
#37113=CARTESIAN_POINT('Ctrl Pts',(108.016869632514,0.743009589010084,339.861802115794));
#37114=CARTESIAN_POINT('Ctrl Pts',(108.009120747486,0.878656719433565,339.841071712494));
#37115=CARTESIAN_POINT('Ctrl Pts',(108.001371862458,1.01339922659645,339.814665632736));
#37116=CARTESIAN_POINT('Ctrl Pts',(107.99362297743,1.14673359920081,339.782696427222));
#37117=CARTESIAN_POINT('Ctrl Pts',(107.985865867655,1.28020949428575,339.750693289263));
#37118=CARTESIAN_POINT('Ctrl Pts',(107.97810875788,1.4122738884897,339.713115321516));
#37119=CARTESIAN_POINT('Ctrl Pts',(107.970351648106,1.54243678443367,339.670125461754));
#37120=CARTESIAN_POINT('Ctrl Pts',(107.96259039318,1.67266923526742,339.627112629586));
#37121=CARTESIAN_POINT('Ctrl Pts',(107.954829138253,1.80099779765773,339.578682280889));
#37122=CARTESIAN_POINT('Ctrl Pts',(107.947067883327,1.92695232127111,339.525045614582));
#37123=CARTESIAN_POINT('Ctrl Pts',(107.939294212923,2.05310833107378,339.471323147089));
#37124=CARTESIAN_POINT('Ctrl Pts',(107.931520542518,2.17688236010878,339.412377887506));
#37125=CARTESIAN_POINT('Ctrl Pts',(107.923746872113,2.29782794561957,339.348467522568));
#37126=CARTESIAN_POINT('Ctrl Pts',(107.916335067936,2.41314348502651,339.287532200495));
#37127=CARTESIAN_POINT('Ctrl Pts',(107.908923263759,2.52588773406848,339.222083766185));
#37128=CARTESIAN_POINT('Ctrl Pts',(107.901511459582,2.63569971460231,339.152381253804));
#37129=CARTESIAN_POINT('Ctrl Pts',(107.893736380804,2.7508939074156,339.079262413658));
#37130=CARTESIAN_POINT('Ctrl Pts',(107.885961302025,2.86322516033814,339.001230872214));
#37131=CARTESIAN_POINT('Ctrl Pts',(107.878186223247,2.97224607350173,338.918537525794));
#37132=CARTESIAN_POINT('Ctrl Pts',(107.870420712198,3.08113282949107,338.835945938801));
#37133=CARTESIAN_POINT('Ctrl Pts',(107.862655201149,3.18671704253944,338.748704195076));
#37134=CARTESIAN_POINT('Ctrl Pts',(107.8548896901,3.28857811712067,338.657107741111));
#37135=CARTESIAN_POINT('Ctrl Pts',(107.847131878578,3.39033819614996,338.565602105297));
#37136=CARTESIAN_POINT('Ctrl Pts',(107.839374067055,3.48838219423739,338.469750611398));
#37137=CARTESIAN_POINT('Ctrl Pts',(107.831616255533,3.58232088949783,338.369890221827));
#37138=CARTESIAN_POINT('Ctrl Pts',(107.82386428201,3.67618889291106,338.270104980366));
#37139=CARTESIAN_POINT('Ctrl Pts',(107.816112308487,3.76595747599722,338.166317131623));
#37140=CARTESIAN_POINT('Ctrl Pts',(107.808360334964,3.85127300798222,338.058901646096));
#37141=CARTESIAN_POINT('Ctrl Pts',(107.800611644407,3.93655240878877,337.95153165109));
#37142=CARTESIAN_POINT('Ctrl Pts',(107.792862953849,4.01738226675829,337.840537380346));
#37143=CARTESIAN_POINT('Ctrl Pts',(107.785114263291,4.0934482756819,337.726327984087));
#37144=CARTESIAN_POINT('Ctrl Pts',(107.777367184913,4.16949845843704,337.612142350047));
#37145=CARTESIAN_POINT('Ctrl Pts',(107.769620106536,4.24078654709393,337.494743246168));
#37146=CARTESIAN_POINT('Ctrl Pts',(107.761873028158,4.3070409774704,337.374569662253));
#37147=CARTESIAN_POINT('Ctrl Pts',(107.754125884852,4.37329596312276,337.254395071167));
#37148=CARTESIAN_POINT('Ctrl Pts',(107.746378741546,4.43451701763259,337.131446295963));
#37149=CARTESIAN_POINT('Ctrl Pts',(107.73863159824,4.4904782436648,337.006187480191));
#37150=CARTESIAN_POINT('Ctrl Pts',(107.730882713212,4.5464520509687,336.880900503577));
#37151=CARTESIAN_POINT('Ctrl Pts',(107.723133828184,4.59716351730095,336.753302809761));
#37152=CARTESIAN_POINT('Ctrl Pts',(107.715384943156,4.6424348100919,336.623878719778));
#37153=CARTESIAN_POINT('Ctrl Pts',(107.707627833381,4.68775415430075,336.494317257728));
#37154=CARTESIAN_POINT('Ctrl Pts',(107.699870723607,4.72762166108901,336.362925896601));
#37155=CARTESIAN_POINT('Ctrl Pts',(107.692113613832,4.7619091826073,336.230204860623));
#37156=CARTESIAN_POINT('Ctrl Pts',(107.684352358906,4.79621502628079,336.097412902767));
#37157=CARTESIAN_POINT('Ctrl Pts',(107.67659110398,4.82493486144602,335.96329023627));
#37158=CARTESIAN_POINT('Ctrl Pts',(107.668829849053,4.847991864457,335.828346512432));
#37159=CARTESIAN_POINT('Ctrl Pts',(107.661056178649,4.87108575115853,335.693186922614));
#37160=CARTESIAN_POINT('Ctrl Pts',(107.653282508244,4.88849865409562,335.557204038756));
#37161=CARTESIAN_POINT('Ctrl Pts',(107.645508837839,4.90020566092802,335.420912749996));
#37162=CARTESIAN_POINT('Ctrl Pts',(107.638097033662,4.91136770377592,335.290965853516));
#37163=CARTESIAN_POINT('Ctrl Pts',(107.630685229485,4.91734310150411,335.160738905966));
#37164=CARTESIAN_POINT('Ctrl Pts',(107.623273425308,4.91815433548213,335.03067563982));
#37165=CARTESIAN_POINT('Ctrl Pts',(107.615498346529,4.91900533045394,334.894237585561));
#37166=CARTESIAN_POINT('Ctrl Pts',(107.607723267751,4.91417582904538,334.757548493972));
#37167=CARTESIAN_POINT('Ctrl Pts',(107.599948188973,4.90363470158705,334.621120367542));
#37168=CARTESIAN_POINT('Ctrl Pts',(107.592182677924,4.89310654565713,334.484860124608));
#37169=CARTESIAN_POINT('Ctrl Pts',(107.584417166875,4.87688077823922,334.348860593855));
#37170=CARTESIAN_POINT('Ctrl Pts',(107.576651655826,4.85497823821829,334.213635346085));
#37171=CARTESIAN_POINT('Ctrl Pts',(107.568893844303,4.83309741462955,334.078544174542));
#37172=CARTESIAN_POINT('Ctrl Pts',(107.561136032781,4.80555108163696,333.944226141567));
#37173=CARTESIAN_POINT('Ctrl Pts',(107.553378221259,4.77241196782509,333.811190901843));
#37174=CARTESIAN_POINT('Ctrl Pts',(107.545626247736,4.73929779224731,333.678255775357));
#37175=CARTESIAN_POINT('Ctrl Pts',(107.537874274213,4.70059930725059,333.54660189841));
#37176=CARTESIAN_POINT('Ctrl Pts',(107.53012230069,4.65644046362301,333.416729564719));
#37177=CARTESIAN_POINT('Ctrl Pts',(107.522373610132,4.61230032129189,333.286912232038));
#37178=CARTESIAN_POINT('Ctrl Pts',(107.514624919575,4.56270454522748,333.158875311293));
#37179=CARTESIAN_POINT('Ctrl Pts',(107.506876229017,4.50782710945783,333.033104523942));
#37180=CARTESIAN_POINT('Ctrl Pts',(107.499129150639,4.45296109139705,332.907359904254));
#37181=CARTESIAN_POINT('Ctrl Pts',(107.491382072261,4.39281575562719,332.78388083817));
#37182=CARTESIAN_POINT('Ctrl Pts',(107.483634993883,4.32761329907645,332.663133252375));
#37183=CARTESIAN_POINT('Ctrl Pts',(107.475887850578,4.26241029606638,332.542384654598));
#37184=CARTESIAN_POINT('Ctrl Pts',(107.468140707272,4.19215027345905,332.424367926705));
#37185=CARTESIAN_POINT('Ctrl Pts',(107.460393563966,4.11710129345659,332.30952420529));
#37186=CARTESIAN_POINT('Ctrl Pts',(107.452644678938,4.04203544085009,332.194654664569));
#37187=CARTESIAN_POINT('Ctrl Pts',(107.44489579391,3.96217870219855,332.082959876971));
#37188=CARTESIAN_POINT('Ctrl Pts',(107.437146908882,3.87784211798493,331.974851479599));
#37189=CARTESIAN_POINT('Ctrl Pts',(107.429389799107,3.79341601804948,331.866628334858));
#37190=CARTESIAN_POINT('Ctrl Pts',(107.421632689332,3.70450081488571,331.761999493123));
#37191=CARTESIAN_POINT('Ctrl Pts',(107.413875579558,3.6114478095638,331.661343416687));
#37192=CARTESIAN_POINT('Ctrl Pts',(107.406114324631,3.51834507969104,331.560633552862));
#37193=CARTESIAN_POINT('Ctrl Pts',(107.398353069705,3.42110041880388,331.463900959963));
#37194=CARTESIAN_POINT('Ctrl Pts',(107.390591814779,3.32010082986982,331.371486042193));
#37195=CARTESIAN_POINT('Ctrl Pts',(107.382818144374,3.21893967450923,331.278923290673));
#37196=CARTESIAN_POINT('Ctrl Pts',(107.37504447397,3.11401188733686,331.190692267954));
#37197=CARTESIAN_POINT('Ctrl Pts',(107.367270803565,3.00573696811573,331.10709255941));
#37198=CARTESIAN_POINT('Ctrl Pts',(107.359858999388,2.90250227243516,331.027384437412));
#37199=CARTESIAN_POINT('Ctrl Pts',(107.352447195211,2.79622528455195,330.951886324245));
#37200=CARTESIAN_POINT('Ctrl Pts',(107.345035391034,2.68729131452731,330.880819443947));
#37201=CARTESIAN_POINT('Ctrl Pts',(107.337260312256,2.57301816613274,330.806269364147));
#37202=CARTESIAN_POINT('Ctrl Pts',(107.329485233477,2.45545987255247,330.736360284237));
#37203=CARTESIAN_POINT('Ctrl Pts',(107.321710154699,2.33503014155402,330.671395455746));
#37204=CARTESIAN_POINT('Ctrl Pts',(107.31394464365,2.21474860700649,330.606510570613));
#37205=CARTESIAN_POINT('Ctrl Pts',(107.306179132601,2.09160300638987,330.546558014855));
#37206=CARTESIAN_POINT('Ctrl Pts',(107.298413621552,1.96603648946314,330.491798187237));
#37207=CARTESIAN_POINT('Ctrl Pts',(107.290655810029,1.84059447210359,330.437092654148));
#37208=CARTESIAN_POINT('Ctrl Pts',(107.282897998507,1.71273667123535,330.387569758427));
#37209=CARTESIAN_POINT('Ctrl Pts',(107.275140186985,1.5829310239641,330.343444144448));
#37210=CARTESIAN_POINT('Ctrl Pts',(107.267388213462,1.45322305955879,330.299351736394));
#37211=CARTESIAN_POINT('Ctrl Pts',(107.259636239939,1.32157053497217,330.26064865091));
#37212=CARTESIAN_POINT('Ctrl Pts',(107.251884266416,1.18846123474575,330.227501392771));
#37213=CARTESIAN_POINT('Ctrl Pts',(107.244135575858,1.05540830638701,330.194368172515));
#37214=CARTESIAN_POINT('Ctrl Pts',(107.236386885301,0.920900207950748,330.166786194114));
#37215=CARTESIAN_POINT('Ctrl Pts',(107.228638194743,0.785439540304255,330.14487201085));
#37216=CARTESIAN_POINT('Ctrl Pts',(107.220891116365,0.650007056381056,330.122962387015));
#37217=CARTESIAN_POINT('Ctrl Pts',(107.213144037988,0.513622783076975,330.106718275122));
#37218=CARTESIAN_POINT('Ctrl Pts',(107.20539695961,0.376798771589208,330.0962049647));
#37219=CARTESIAN_POINT('Ctrl Pts',(107.197649816304,0.23997361338444,330.085691566167));
#37220=CARTESIAN_POINT('Ctrl Pts',(107.189902672998,0.102709099370616,330.080909094847));
#37221=CARTESIAN_POINT('Ctrl Pts',(107.182155529692,-0.0344787454392194,
330.081870855842));
#37222=CARTESIAN_POINT('Ctrl Pts',(107.174406644664,-0.171697432989055,
330.082832833062));
#37223=CARTESIAN_POINT('Ctrl Pts',(107.166657759636,-0.308839026247162,
330.089541609647));
#37224=CARTESIAN_POINT('Ctrl Pts',(107.158908874608,-0.445389048938188,
330.101958385478));
#37225=CARTESIAN_POINT('Ctrl Pts',(107.151151764833,-0.582084007234216,
330.114388340604));
#37226=CARTESIAN_POINT('Ctrl Pts',(107.143394655059,-0.718185750792701,
330.132538362002));
#37227=CARTESIAN_POINT('Ctrl Pts',(107.135637545284,-0.853185913430837,
330.156317840772));
#37228=CARTESIAN_POINT('Ctrl Pts',(107.127876290358,-0.988258215839419,
330.180110026535));
#37229=CARTESIAN_POINT('Ctrl Pts',(107.120115035431,-1.12222738281142,330.209537579966));
#37230=CARTESIAN_POINT('Ctrl Pts',(107.112353780505,-1.25459773167696,330.24445927426));
#37231=CARTESIAN_POINT('Ctrl Pts',(107.104580110101,-1.38717982996129,330.279436831884));
#37232=CARTESIAN_POINT('Ctrl Pts',(107.096806439696,-1.51815762568644,330.319925977565));
#37233=CARTESIAN_POINT('Ctrl Pts',(107.089032769291,-1.64705217572689,330.365736067838));
#37234=CARTESIAN_POINT('Ctrl Pts',(107.081620965114,-1.76994665345263,330.409413687388));
#37235=CARTESIAN_POINT('Ctrl Pts',(107.074209160937,-1.89094720381393,330.457927912704));
#37236=CARTESIAN_POINT('Ctrl Pts',(107.06679735676,-2.00965928141386,330.511074445357));
#37237=CARTESIAN_POINT('Ctrl Pts',(107.059022277982,-2.134189791562,330.56682584789));
#37238=CARTESIAN_POINT('Ctrl Pts',(107.051247199203,-2.25659536645293,330.627851310436));
#37239=CARTESIAN_POINT('Ctrl Pts',(107.043472120425,-2.37639711439414,330.693967044111));
#37240=CARTESIAN_POINT('Ctrl Pts',(107.035706609376,-2.49605143865748,330.760001418167));
#37241=CARTESIAN_POINT('Ctrl Pts',(107.027941098327,-2.61310797241295,330.831113412924));
#37242=CARTESIAN_POINT('Ctrl Pts',(107.020175587278,-2.72710792702054,330.907071291009));
#37243=CARTESIAN_POINT('Ctrl Pts',(107.012417775756,-2.84099485034124,330.982953856637));
#37244=CARTESIAN_POINT('Ctrl Pts',(107.004659964234,-2.95183090240648,331.063672528616));
#37245=CARTESIAN_POINT('Ctrl Pts',(106.996902152711,-3.05918235656461,331.148949965038));
#37246=CARTESIAN_POINT('Ctrl Pts',(106.989150179188,-3.16645302534911,331.234163227484));
#37247=CARTESIAN_POINT('Ctrl Pts',(106.981398205665,-3.27024401090058,331.323928183754));
#37248=CARTESIAN_POINT('Ctrl Pts',(106.973646232142,-3.37015132759812,331.417924750708));
#37249=CARTESIAN_POINT('Ctrl Pts',(106.965897541585,-3.47001633348772,331.511881510061));
#37250=CARTESIAN_POINT('Ctrl Pts',(106.958148851027,-3.56600065769723,331.610066048474));
#37251=CARTESIAN_POINT('Ctrl Pts',(106.95040016047,-3.65773430191766,331.712118791824));
#37252=CARTESIAN_POINT('Ctrl Pts',(106.942653082092,-3.74944886018737,331.814150302249));
#37253=CARTESIAN_POINT('Ctrl Pts',(106.934906003714,-3.83691423644332,331.92004812627));
#37254=CARTESIAN_POINT('Ctrl Pts',(106.927158925336,-3.91979842704514,332.029417001019));
#37255=CARTESIAN_POINT('Ctrl Pts',(106.91941178203,-4.00268331229625,332.138786792385));
#37256=CARTESIAN_POINT('Ctrl Pts',(106.911664638725,-4.08098669922714,332.25162738098));
#37257=CARTESIAN_POINT('Ctrl Pts',(106.903917495419,-4.15441814855179,332.367512030515));
#37258=CARTESIAN_POINT('Ctrl Pts',(106.896168610391,-4.2278661068252,332.483422733379));
#37259=CARTESIAN_POINT('Ctrl Pts',(106.888419725363,-4.29643973876372,332.602378528898));
#37260=CARTESIAN_POINT('Ctrl Pts',(106.880670840335,-4.35989325958387,332.723925786022));
#37261=CARTESIAN_POINT('Ctrl Pts',(106.87291373056,-4.42341413062661,332.845602054661));
#37262=CARTESIAN_POINT('Ctrl Pts',(106.865156620785,-4.48180385337479,332.969874932449));
#37263=CARTESIAN_POINT('Ctrl Pts',(106.85739951101,-4.53486351667543,333.096267889742));
#37264=CARTESIAN_POINT('Ctrl Pts',(106.849638256084,-4.58795153336361,333.22272838739));
#37265=CARTESIAN_POINT('Ctrl Pts',(106.841877001158,-4.63570367927216,333.351310855718));
#37266=CARTESIAN_POINT('Ctrl Pts',(106.834115746232,-4.67797047269869,333.481522038665));
#37267=CARTESIAN_POINT('Ctrl Pts',(106.826342075827,-4.72030487921998,333.61194151707));
#37268=CARTESIAN_POINT('Ctrl Pts',(106.818568405423,-4.75713629359026,333.743994539778));
#37269=CARTESIAN_POINT('Ctrl Pts',(106.810794735018,-4.78836584835855,333.877175185181));
#37270=CARTESIAN_POINT('Ctrl Pts',(106.803382930841,-4.81814165983935,334.0041562395));
#37271=CARTESIAN_POINT('Ctrl Pts',(106.795971126664,-4.84282535357643,334.132162014798));
#37272=CARTESIAN_POINT('Ctrl Pts',(106.788559322486,-4.86237521732448,334.26075017183));
#37273=CARTESIAN_POINT('Ctrl Pts',(106.775427117146,-4.89701358862873,334.488582160125));
#37274=CARTESIAN_POINT('Ctrl Pts',(106.762294911805,-4.91564487213602,334.718907368115));
#37275=CARTESIAN_POINT('Ctrl Pts',(106.749162706464,-4.91799551195798,334.949967941666));
#37276=CARTESIAN_POINT('Ctrl Pts',(106.748287220473,-4.91815222228817,334.965372079057));
#37277=CARTESIAN_POINT('Ctrl Pts',(106.747411734481,-4.91823658492966,334.980779468144));
#37278=CARTESIAN_POINT('Ctrl Pts',(106.74653624849,-4.91824852393596,334.996189579852));
#37279=CARTESIAN_POINT('',(110.24653624849,-4.91461063079939,335.001894868956));
#37280=CARTESIAN_POINT('Ctrl Pts',(110.24653624849,-4.9182496344383,335.001896272004));
#37281=CARTESIAN_POINT('Ctrl Pts',(110.238131601278,-4.91819212410279,335.151057460917));
#37282=CARTESIAN_POINT('Ctrl Pts',(110.229726954067,-4.91134478705064,335.300008991737));
#37283=CARTESIAN_POINT('Ctrl Pts',(110.221322306855,-4.89778963213231,335.448151516652));
#37284=CARTESIAN_POINT('Ctrl Pts',(110.212881585518,-4.8841762962643,335.596929893597));
#37285=CARTESIAN_POINT('Ctrl Pts',(110.204440864181,-4.86379752081166,335.744892036098));
#37286=CARTESIAN_POINT('Ctrl Pts',(110.196000142844,-4.8367869983973,335.891445228062));
#37287=CARTESIAN_POINT('Ctrl Pts',(110.187541124662,-4.80971792561422,336.038316101532));
#37288=CARTESIAN_POINT('Ctrl Pts',(110.17908210648,-4.77598844349376,336.183771654938));
#37289=CARTESIAN_POINT('Ctrl Pts',(110.170623088298,-4.73578228833357,336.327233656899));
#37290=CARTESIAN_POINT('Ctrl Pts',(110.162136028151,-4.69544284825189,336.471171240811));
#37291=CARTESIAN_POINT('Ctrl Pts',(110.153648968005,-4.64858385138581,336.613101785076));
#37292=CARTESIAN_POINT('Ctrl Pts',(110.145161907858,-4.59543845833362,336.752463534048));
#37293=CARTESIAN_POINT('Ctrl Pts',(110.139246516497,-4.55839668019884,336.849597202452));
#37294=CARTESIAN_POINT('Ctrl Pts',(110.133331125135,-4.51830200299678,336.945483427693));
#37295=CARTESIAN_POINT('Ctrl Pts',(110.127415733774,-4.47524643769942,337.039939308989));
#37296=CARTESIAN_POINT('Ctrl Pts',(110.119640654995,-4.41865501515803,337.164090336922));
#37297=CARTESIAN_POINT('Ctrl Pts',(110.111865576217,-4.35680400840861,337.286080848059));
#37298=CARTESIAN_POINT('Ctrl Pts',(110.104090497439,-4.2898804373959,337.40543320326));
#37299=CARTESIAN_POINT('Ctrl Pts',(110.09632498639,-4.22303922009794,337.52463868779));
#37300=CARTESIAN_POINT('Ctrl Pts',(110.088559475341,-4.15113804789479,337.641212138151));
#37301=CARTESIAN_POINT('Ctrl Pts',(110.080793964292,-4.07441175231475,337.754696341723));
#37302=CARTESIAN_POINT('Ctrl Pts',(110.073036152769,-3.99776153108016,337.868068025376));
#37303=CARTESIAN_POINT('Ctrl Pts',(110.065278341247,-3.91629592466286,337.978356236054));
#37304=CARTESIAN_POINT('Ctrl Pts',(110.057520529725,-3.83029519877422,338.085129130644));
#37305=CARTESIAN_POINT('Ctrl Pts',(110.049768556202,-3.74435919115911,338.191821675245));
#37306=CARTESIAN_POINT('Ctrl Pts',(110.042016582679,-3.65389510132756,338.295003866086));
#37307=CARTESIAN_POINT('Ctrl Pts',(110.034264609156,-3.55922573432606,338.394273889157));
#37308=CARTESIAN_POINT('Ctrl Pts',(110.026515918598,-3.46459645985764,338.493501871314));
#37309=CARTESIAN_POINT('Ctrl Pts',(110.018767228041,-3.36576571957422,338.58882069869));
#37310=CARTESIAN_POINT('Ctrl Pts',(110.011018537483,-3.26309557899603,338.6798628106));
#37311=CARTESIAN_POINT('Ctrl Pts',(110.003271459105,-3.1604467997981,338.770885980438));
#37312=CARTESIAN_POINT('Ctrl Pts',(109.995524380728,-3.05396050148425,338.857633945528));
#37313=CARTESIAN_POINT('Ctrl Pts',(109.98777730235,-2.94403418082203,338.939777380088));
#37314=CARTESIAN_POINT('Ctrl Pts',(109.980030159044,-2.83410693887145,339.021921503089));
#37315=CARTESIAN_POINT('Ctrl Pts',(109.972283015738,-2.72073993017841,339.099460784613));
#37316=CARTESIAN_POINT('Ctrl Pts',(109.964535872432,-2.60436184341858,339.17210767491));
#37317=CARTESIAN_POINT('Ctrl Pts',(109.956786987404,-2.48795759239406,339.244770897771));
#37318=CARTESIAN_POINT('Ctrl Pts',(109.949038102376,-2.36854124774976,339.31253933376));
#37319=CARTESIAN_POINT('Ctrl Pts',(109.941289217348,-2.24656809063275,339.375170268304));
#37320=CARTESIAN_POINT('Ctrl Pts',(109.933532107573,-2.12446546994647,339.437867679969));
#37321=CARTESIAN_POINT('Ctrl Pts',(109.925774997799,-1.99980096392575,339.495416518489));
#37322=CARTESIAN_POINT('Ctrl Pts',(109.918017888024,-1.87305243512715,339.547621096548));
#37323=CARTESIAN_POINT('Ctrl Pts',(109.910256633098,-1.74623617596738,339.599853571063));
#37324=CARTESIAN_POINT('Ctrl Pts',(109.902495378172,-1.61733404215803,339.646735961142));
#37325=CARTESIAN_POINT('Ctrl Pts',(109.894734123245,-1.48684028835761,339.688122120787));
#37326=CARTESIAN_POINT('Ctrl Pts',(109.886960452841,-1.35613778707902,339.729574484801));
#37327=CARTESIAN_POINT('Ctrl Pts',(109.879186782436,-1.22383895540408,339.765512946487));
#37328=CARTESIAN_POINT('Ctrl Pts',(109.871413112032,-1.09045037131715,339.795842058512));
#37329=CARTESIAN_POINT('Ctrl Pts',(109.864001307854,-0.963271057909453,
339.824759343076));
#37330=CARTESIAN_POINT('Ctrl Pts',(109.856589503677,-0.835101447788344,
339.848577703379));
#37331=CARTESIAN_POINT('Ctrl Pts',(109.8491776995,-0.706384151899945,339.867258416444));
#37332=CARTESIAN_POINT('Ctrl Pts',(109.841402620722,-0.571358037912271,
339.886854726903));
#37333=CARTESIAN_POINT('Ctrl Pts',(109.833627541943,-0.435302485781498,
339.900858961184));
#37334=CARTESIAN_POINT('Ctrl Pts',(109.825852463165,-0.298720359673227,
339.909169910404));
#37335=CARTESIAN_POINT('Ctrl Pts',(109.818086952116,-0.162306306566375,
339.917470632472));
#37336=CARTESIAN_POINT('Ctrl Pts',(109.810321441067,-0.0253673552049586,
339.920091985795));
#37337=CARTESIAN_POINT('Ctrl Pts',(109.802555930018,0.111584933750508,339.916984021233));
#37338=CARTESIAN_POINT('Ctrl Pts',(109.794798118495,0.24840143411275,339.913879138227));
#37339=CARTESIAN_POINT('Ctrl Pts',(109.787040306973,0.385230857495597,339.905056250932));
#37340=CARTESIAN_POINT('Ctrl Pts',(109.779282495451,0.521558389955213,339.890517345677));
#37341=CARTESIAN_POINT('Ctrl Pts',(109.771530521928,0.657783331623366,339.875989381409));
#37342=CARTESIAN_POINT('Ctrl Pts',(109.763778548405,0.793506747034172,339.85575400236));
#37343=CARTESIAN_POINT('Ctrl Pts',(109.756026574882,0.928216053879054,339.829865217563));
#37344=CARTESIAN_POINT('Ctrl Pts',(109.748277884324,1.06286831125251,339.80398739668));
#37345=CARTESIAN_POINT('Ctrl Pts',(109.740529193767,1.1965069312056,339.772461005601));
#37346=CARTESIAN_POINT('Ctrl Pts',(109.732780503209,1.32862688968728,339.735391604767));
#37347=CARTESIAN_POINT('Ctrl Pts',(109.725033424831,1.4607193595082,339.698329916532));
#37348=CARTESIAN_POINT('Ctrl Pts',(109.717286346453,1.59129342023932,339.655727618001));
#37349=CARTESIAN_POINT('Ctrl Pts',(109.709539268076,1.71985702649545,339.607740755611));
#37350=CARTESIAN_POINT('Ctrl Pts',(109.70179212477,1.84842171023827,339.559753491044));
#37351=CARTESIAN_POINT('Ctrl Pts',(109.694044981464,1.97497553970162,339.506381709291));
#37352=CARTESIAN_POINT('Ctrl Pts',(109.686297838158,2.09904472012501,339.447830294134));
#37353=CARTESIAN_POINT('Ctrl Pts',(109.67854895313,2.22314179393413,339.389265715376));
#37354=CARTESIAN_POINT('Ctrl Pts',(109.670800068102,2.34475275372905,339.325519352794));
#37355=CARTESIAN_POINT('Ctrl Pts',(109.663051183074,2.46342711689372,339.256842715235));
#37356=CARTESIAN_POINT('Ctrl Pts',(109.655294073299,2.58222744225374,339.188093183584));
#37357=CARTESIAN_POINT('Ctrl Pts',(109.647536963524,2.69808460577164,339.114403119545));
#37358=CARTESIAN_POINT('Ctrl Pts',(109.63977985375,2.81057545095884,339.036068470302));
#37359=CARTESIAN_POINT('Ctrl Pts',(109.632018598824,2.92312640765686,338.957691961528));
#37360=CARTESIAN_POINT('Ctrl Pts',(109.624257343897,3.0323071506728,338.874666158583));
#37361=CARTESIAN_POINT('Ctrl Pts',(109.616496088971,3.13772731316523,338.787327602772));
#37362=CARTESIAN_POINT('Ctrl Pts',(109.608722418567,3.24331611356129,338.699849333735));
#37363=CARTESIAN_POINT('Ctrl Pts',(109.600948748162,3.34513202183141,338.608044787474));
#37364=CARTESIAN_POINT('Ctrl Pts',(109.593175077757,3.44282063586128,338.512288304195));
#37365=CARTESIAN_POINT('Ctrl Pts',(109.58576327358,3.53596182140487,338.420989308252));
#37366=CARTESIAN_POINT('Ctrl Pts',(109.578351469403,3.62535111913162,338.326098230181));
#37367=CARTESIAN_POINT('Ctrl Pts',(109.570939665226,3.71071644388418,338.227966315746));
#37368=CARTESIAN_POINT('Ctrl Pts',(109.563164586448,3.80026577749375,338.125024663863));
#37369=CARTESIAN_POINT('Ctrl Pts',(109.555389507669,3.88566970299204,338.018191142191));
#37370=CARTESIAN_POINT('Ctrl Pts',(109.547614428891,3.96657098301511,337.907833849999));
#37371=CARTESIAN_POINT('Ctrl Pts',(109.539848917842,4.04737270886268,337.797612359482));
#37372=CARTESIAN_POINT('Ctrl Pts',(109.532083406793,4.12368258493346,337.683876038514));
#37373=CARTESIAN_POINT('Ctrl Pts',(109.524317895744,4.19518177310224,337.567028039023));
#37374=CARTESIAN_POINT('Ctrl Pts',(109.516560084222,4.26661006961778,337.450295894664));
#37375=CARTESIAN_POINT('Ctrl Pts',(109.508802272699,4.33323696772656,337.330458542841));
#37376=CARTESIAN_POINT('Ctrl Pts',(109.501044461177,4.39478554240987,337.2079499765));
#37377=CARTESIAN_POINT('Ctrl Pts',(109.493292487654,4.45628779983887,337.08553360174));
#37378=CARTESIAN_POINT('Ctrl Pts',(109.485540514131,4.51271916578058,336.96045036148));
#37379=CARTESIAN_POINT('Ctrl Pts',(109.477788540608,4.56384766988322,336.833160524504));
#37380=CARTESIAN_POINT('Ctrl Pts',(109.47003985005,4.61495452103402,336.705924594851));
#37381=CARTESIAN_POINT('Ctrl Pts',(109.462291159493,4.66076283162849,336.57648428908));
#37382=CARTESIAN_POINT('Ctrl Pts',(109.454542468935,4.70108807220229,336.445321417505));
#37383=CARTESIAN_POINT('Ctrl Pts',(109.446795390557,4.741404922773,336.314185835459));
#37384=CARTESIAN_POINT('Ctrl Pts',(109.43904831218,4.77624085765821,336.181328773861));
#37385=CARTESIAN_POINT('Ctrl Pts',(109.431301233802,4.80546082564253,336.047248449851));
#37386=CARTESIAN_POINT('Ctrl Pts',(109.423554090496,4.8346810385183,335.913167002119));
#37387=CARTESIAN_POINT('Ctrl Pts',(109.41580694719,4.85828510738479,335.777862653436));
#37388=CARTESIAN_POINT('Ctrl Pts',(109.408059803884,4.87618892585517,335.641844702298));
#37389=CARTESIAN_POINT('Ctrl Pts',(109.400310918856,4.89409676948403,335.505796171436));
#37390=CARTESIAN_POINT('Ctrl Pts',(109.392562033828,4.90630176160053,335.36903410633));
#37391=CARTESIAN_POINT('Ctrl Pts',(109.3848131488,4.91277161936732,335.23207343329));
#37392=CARTESIAN_POINT('Ctrl Pts',(109.377056039025,4.91924834430799,335.094967388777));
#37393=CARTESIAN_POINT('Ctrl Pts',(109.369298929251,4.91997775641148,334.957662706284));
#37394=CARTESIAN_POINT('Ctrl Pts',(109.361541819476,4.91497972972099,334.820675381133));
#37395=CARTESIAN_POINT('Ctrl Pts',(109.35378056455,4.90997903224484,334.683614854335));
#37396=CARTESIAN_POINT('Ctrl Pts',(109.346019309623,4.89924482810669,334.546872412271));
#37397=CARTESIAN_POINT('Ctrl Pts',(109.338258054697,4.88284887217082,334.410958444556));
#37398=CARTESIAN_POINT('Ctrl Pts',(109.330484384293,4.86642668804888,334.274827058786));
#37399=CARTESIAN_POINT('Ctrl Pts',(109.322710713888,4.84432471669487,334.139527181649));
#37400=CARTESIAN_POINT('Ctrl Pts',(109.314937043483,4.81666596145387,334.005559414408));
#37401=CARTESIAN_POINT('Ctrl Pts',(109.307525239306,4.7902947279236,333.877827878963));
#37402=CARTESIAN_POINT('Ctrl Pts',(109.300113435129,4.75887247411791,333.751307504273));
#37403=CARTESIAN_POINT('Ctrl Pts',(109.292701630952,4.72254732920113,333.626417171789));
#37404=CARTESIAN_POINT('Ctrl Pts',(109.284926552173,4.68444178072505,333.495405592081));
#37405=CARTESIAN_POINT('Ctrl Pts',(109.277151473395,4.64082015772091,333.365773860434));
#37406=CARTESIAN_POINT('Ctrl Pts',(109.269376394617,4.5917986810825,333.238021585005));
#37407=CARTESIAN_POINT('Ctrl Pts',(109.261610883568,4.54283752849195,333.110426516883));
#37408=CARTESIAN_POINT('Ctrl Pts',(109.253845372519,4.48848988233381,332.984706664631));
#37409=CARTESIAN_POINT('Ctrl Pts',(109.24607986147,4.42892222005965,332.861348314671));
#37410=CARTESIAN_POINT('Ctrl Pts',(109.238322049947,4.36941361929606,332.738112274873));
#37411=CARTESIAN_POINT('Ctrl Pts',(109.230564238425,4.30469547114769,332.617233427494));
#37412=CARTESIAN_POINT('Ctrl Pts',(109.222806426903,4.23498286952324,332.499179503174));
#37413=CARTESIAN_POINT('Ctrl Pts',(109.21505445338,4.16532272884222,332.381214418176));
#37414=CARTESIAN_POINT('Ctrl Pts',(109.207302479857,4.09067581371561,332.266070360066));
#37415=CARTESIAN_POINT('Ctrl Pts',(109.199550506334,4.01130364151637,332.15419147551));
#37416=CARTESIAN_POINT('Ctrl Pts',(109.191801815776,3.93196508347924,332.042359971729));
#37417=CARTESIAN_POINT('Ctrl Pts',(109.184053125219,3.84790547421205,331.933791209337));
#37418=CARTESIAN_POINT('Ctrl Pts',(109.176304434661,3.75943011880288,331.828901098304));
#37419=CARTESIAN_POINT('Ctrl Pts',(109.168557356283,3.67097317143031,331.724032810534));
#37420=CARTESIAN_POINT('Ctrl Pts',(109.160810277905,3.57810255720293,331.62284195033));
#37421=CARTESIAN_POINT('Ctrl Pts',(109.153063199527,3.48116415358215,331.525711699022));
#37422=CARTESIAN_POINT('Ctrl Pts',(109.145316056222,3.38422493752432,331.428580633669));
#37423=CARTESIAN_POINT('Ctrl Pts',(109.137568912916,3.28321814019055,331.335510521755));
#37424=CARTESIAN_POINT('Ctrl Pts',(109.12982176961,3.17852652675748,331.246847700772));
#37425=CARTESIAN_POINT('Ctrl Pts',(109.122072884582,3.07381137642705,331.158164946505));
#37426=CARTESIAN_POINT('Ctrl Pts',(109.114323999554,2.96541005974504,331.073891707418));
#37427=CARTESIAN_POINT('Ctrl Pts',(109.106575114526,2.85373811913615,330.99433378701));
#37428=CARTESIAN_POINT('Ctrl Pts',(109.098818004751,2.74194764877562,330.914691423003));
#37429=CARTESIAN_POINT('Ctrl Pts',(109.091060894976,2.62687993874335,330.839774602566));
#37430=CARTESIAN_POINT('Ctrl Pts',(109.083303785202,2.5089796554982,330.769845847868));
#37431=CARTESIAN_POINT('Ctrl Pts',(109.075542530275,2.39101637011147,330.69987972548));
#37432=CARTESIAN_POINT('Ctrl Pts',(109.067781275349,2.27021783952015,330.634907165063));
#37433=CARTESIAN_POINT('Ctrl Pts',(109.060020020423,2.14705209191434,330.57514402753));
#37434=CARTESIAN_POINT('Ctrl Pts',(109.052246350018,2.02368931925198,330.515285288453));
#37435=CARTESIAN_POINT('Ctrl Pts',(109.044472679614,1.89795212116079,330.460652780665));
#37436=CARTESIAN_POINT('Ctrl Pts',(109.036699009209,1.77032802809097,330.411413972098));
#37437=CARTESIAN_POINT('Ctrl Pts',(109.029287205032,1.64864486725917,330.364467241917));
#37438=CARTESIAN_POINT('Ctrl Pts',(109.021875400855,1.5252468004473,330.322423451024));
#37439=CARTESIAN_POINT('Ctrl Pts',(109.014463596678,1.40056623519365,330.285384715235));
#37440=CARTESIAN_POINT('Ctrl Pts',(109.006688517899,1.26977470403156,330.246530600672));
#37441=CARTESIAN_POINT('Ctrl Pts',(108.998913439121,1.13715845210191,330.213061785822));
#37442=CARTESIAN_POINT('Ctrl Pts',(108.991138360343,1.00320050435739,330.185150904695));
#37443=CARTESIAN_POINT('Ctrl Pts',(108.983372849294,0.869407400395848,330.157274369685));
#37444=CARTESIAN_POINT('Ctrl Pts',(108.975607338245,0.734276264718385,330.134942238938));
#37445=CARTESIAN_POINT('Ctrl Pts',(108.967841827196,0.598306116453239,330.118277675501));
#37446=CARTESIAN_POINT('Ctrl Pts',(108.960084015673,0.462470782985871,330.101629635026));
#37447=CARTESIAN_POINT('Ctrl Pts',(108.952326204151,0.325798477897935,330.090638026161));
#37448=CARTESIAN_POINT('Ctrl Pts',(108.944568392629,0.188798925520283,330.085375087738));
#37449=CARTESIAN_POINT('Ctrl Pts',(108.936816419106,0.0519024696503939,
330.080116109843));
#37450=CARTESIAN_POINT('Ctrl Pts',(108.929064445583,-0.0853203543193356,
330.080577236487));
#37451=CARTESIAN_POINT('Ctrl Pts',(108.92131247206,-0.222354531924368,330.086778905379));
#37452=CARTESIAN_POINT('Ctrl Pts',(108.913563781502,-0.359330675473921,
330.09297794786));
#37453=CARTESIAN_POINT('Ctrl Pts',(108.905815090945,-0.496117941896057,
330.104912679621));
#37454=CARTESIAN_POINT('Ctrl Pts',(108.898066400387,-0.632201365523266,
330.12255143585));
#37455=CARTESIAN_POINT('Ctrl Pts',(108.890319322009,-0.768256475857506,
330.140186522188));
#37456=CARTESIAN_POINT('Ctrl Pts',(108.882572243631,-0.903607647288817,
330.163523222213));
#37457=CARTESIAN_POINT('Ctrl Pts',(108.874825165254,-1.03774548032018,330.192478041592));
#37458=CARTESIAN_POINT('Ctrl Pts',(108.867078021948,-1.1718844375557,330.221433103641));
#37459=CARTESIAN_POINT('Ctrl Pts',(108.859330878642,-1.30480965403428,330.256006296485));
#37460=CARTESIAN_POINT('Ctrl Pts',(108.851583735336,-1.43602275096882,330.296063167814));
#37461=CARTESIAN_POINT('Ctrl Pts',(108.843834850308,-1.56726534739338,330.336129044777));
#37462=CARTESIAN_POINT('Ctrl Pts',(108.83608596528,-1.69679468455561,330.381680939348));
#37463=CARTESIAN_POINT('Ctrl Pts',(108.828337080252,-1.82412873191852,330.432534900857));
#37464=CARTESIAN_POINT('Ctrl Pts',(108.820579970477,-1.95159793295482,330.483442839286));
#37465=CARTESIAN_POINT('Ctrl Pts',(108.812822860702,-2.07686682602267,330.53966394125));
#37466=CARTESIAN_POINT('Ctrl Pts',(108.805065750928,-2.19947401609355,330.600966343044));
#37467=CARTESIAN_POINT('Ctrl Pts',(108.797304496001,-2.32214672352659,330.662301502882));
#37468=CARTESIAN_POINT('Ctrl Pts',(108.789543241075,-2.44215455203073,330.728723183814));
#37469=CARTESIAN_POINT('Ctrl Pts',(108.781781986149,-2.559062702652,330.799954625674));
#37470=CARTESIAN_POINT('Ctrl Pts',(108.774008315744,-2.67615786821398,330.871300014627));
#37471=CARTESIAN_POINT('Ctrl Pts',(108.76623464534,-2.790143122232,330.947470322211));
#37472=CARTESIAN_POINT('Ctrl Pts',(108.758460974935,-2.90061380664893,331.028146200176));
#37473=CARTESIAN_POINT('Ctrl Pts',(108.751049170758,-3.00594205412869,331.105066596612));
#37474=CARTESIAN_POINT('Ctrl Pts',(108.743637366581,-3.10807534938728,331.186082355853));
#37475=CARTESIAN_POINT('Ctrl Pts',(108.736225562404,-3.20669382052801,331.270885117902));
#37476=CARTESIAN_POINT('Ctrl Pts',(108.728562913846,-3.30864992563361,331.358557936397));
#37477=CARTESIAN_POINT('Ctrl Pts',(108.720900265287,-3.40719142055373,331.450573305663));
#37478=CARTESIAN_POINT('Ctrl Pts',(108.713237616729,-3.50191761917469,331.546631202577));
#37479=CARTESIAN_POINT('Ctrl Pts',(108.705584462041,-3.59652645390365,331.642570085651));
#37480=CARTESIAN_POINT('Ctrl Pts',(108.697931307353,-3.68732911260994,331.742541251977));
#37481=CARTESIAN_POINT('Ctrl Pts',(108.690278152666,-3.77395733333042,331.846204015999));
#37482=CARTESIAN_POINT('Ctrl Pts',(108.682632523285,-3.86050037297028,331.949764848962));
#37483=CARTESIAN_POINT('Ctrl Pts',(108.674986893905,-3.94287688229336,332.057009752153));
#37484=CARTESIAN_POINT('Ctrl Pts',(108.667341264524,-4.02075527324775,332.167561104781));
#37485=CARTESIAN_POINT('Ctrl Pts',(108.659701345131,-4.0985755022631,332.278029894313));
#37486=CARTESIAN_POINT('Ctrl Pts',(108.652061425738,-4.17190406617584,332.391799891288));
#37487=CARTESIAN_POINT('Ctrl Pts',(108.644421506345,-4.24044987896429,332.508460739524));
#37488=CARTESIAN_POINT('Ctrl Pts',(108.636784588332,-4.30896876319232,332.625075756972));
#37489=CARTESIAN_POINT('Ctrl Pts',(108.629147670319,-4.37270842827463,332.744579020613));
#37490=CARTESIAN_POINT('Ctrl Pts',(108.621510752306,-4.43142153970922,332.866531884489));
#37491=CARTESIAN_POINT('Ctrl Pts',(108.613875070075,-4.49012515037309,332.988465014337));
#37492=CARTESIAN_POINT('Ctrl Pts',(108.606239387844,-4.54380365076244,333.112846592724));
#37493=CARTESIAN_POINT('Ctrl Pts',(108.598603705613,-4.59225629740001,333.239214617993));
#37494=CARTESIAN_POINT('Ctrl Pts',(108.590967494843,-4.6407122979124,333.365591390411));
#37495=CARTESIAN_POINT('Ctrl Pts',(108.583331284073,-4.68394158254028,333.493954506195));
#37496=CARTESIAN_POINT('Ctrl Pts',(108.575695073302,-4.72179226687599,333.623823829966));
#37497=CARTESIAN_POINT('Ctrl Pts',(108.568053090257,-4.75967156285829,333.753791323037));
#37498=CARTESIAN_POINT('Ctrl Pts',(108.560411107212,-4.79216402805422,333.885266909895));
#37499=CARTESIAN_POINT('Ctrl Pts',(108.552769124166,-4.81916817768044,334.017757088225));
#37500=CARTESIAN_POINT('Ctrl Pts',(108.545123862112,-4.84618391420262,334.150304115222));
#37501=CARTESIAN_POINT('Ctrl Pts',(108.537478600057,-4.86770658117338,334.283866203063));
#37502=CARTESIAN_POINT('Ctrl Pts',(108.529833338002,-4.88368637289488,334.417942894811));
#37503=CARTESIAN_POINT('Ctrl Pts',(108.522178982304,-4.89968517175085,334.552179063838));
#37504=CARTESIAN_POINT('Ctrl Pts',(108.514524626606,-4.91012790262292,334.68693065758));
#37505=CARTESIAN_POINT('Ctrl Pts',(108.506870270908,-4.91501683048537,334.821695152771));
#37506=CARTESIAN_POINT('Ctrl Pts',(108.50342559678,-4.91721698474864,334.882342944469));
#37507=CARTESIAN_POINT('Ctrl Pts',(108.499980922652,-4.91829305663433,334.942993382303));
#37508=CARTESIAN_POINT('Ctrl Pts',(108.496536248524,-4.9182486817404,335.003600980256));
#37509=CARTESIAN_POINT('',(111.99653624849,-4.91682066856926,334.995613600539));
#37510=CARTESIAN_POINT('Ctrl Pts',(111.99653624849,-4.91583883843042,334.99561447645));
#37511=CARTESIAN_POINT('Ctrl Pts',(111.929972145466,-4.90575025587869,336.172136823171));
#37512=CARTESIAN_POINT('Ctrl Pts',(111.770662031017,-3.8923044058229,339.00355018297));
#37513=CARTESIAN_POINT('Ctrl Pts',(111.518605905143,0.841275660426242,340.754711472316));
#37514=CARTESIAN_POINT('Ctrl Pts',(111.240367870869,5.29452218069954,337.406757932263));
#37515=CARTESIAN_POINT('Ctrl Pts',(110.962129836596,4.88906384276416,331.850158161461));
#37516=CARTESIAN_POINT('Ctrl Pts',(110.683891802322,-0.00301622121185956,
329.184121754297));
#37517=CARTESIAN_POINT('Ctrl Pts',(110.445360606286,-4.19458360114431,331.474041886394));
#37518=CARTESIAN_POINT('Ctrl Pts',(110.299575421676,-4.90756129070927,334.062005703542));
#37519=CARTESIAN_POINT('Ctrl Pts',(110.24653624849,-4.91080622874904,335.001893402137));
#37520=CARTESIAN_POINT('',(113.746536248529,-4.91824999495766,335.000222708279));
#37521=CARTESIAN_POINT('Ctrl Pts',(113.74653624849,-4.91824999495763,335.000222708968));
#37522=CARTESIAN_POINT('Ctrl Pts',(113.745860892105,-4.91824945829249,335.012074289756));
#37523=CARTESIAN_POINT('Ctrl Pts',(113.74518553572,-4.91820608331596,335.023925756962));
#37524=CARTESIAN_POINT('Ctrl Pts',(113.744510179335,-4.91811987196888,335.035776912175));
#37525=CARTESIAN_POINT('Ctrl Pts',(113.736735100557,-4.91712735893421,335.172214010356));
#37526=CARTESIAN_POINT('Ctrl Pts',(113.728960021778,-4.91045147623641,335.308825373111));
#37527=CARTESIAN_POINT('Ctrl Pts',(113.721184943,-4.89806801477245,335.445098624086));
#37528=CARTESIAN_POINT('Ctrl Pts',(113.713419431951,-4.88569979194618,335.58120418215));
#37529=CARTESIAN_POINT('Ctrl Pts',(113.705653920902,-4.86763800021826,335.716972070743));
#37530=CARTESIAN_POINT('Ctrl Pts',(113.697888409853,-4.84391041548599,335.851889047498));
#37531=CARTESIAN_POINT('Ctrl Pts',(113.69013059833,-4.82020635672306,335.986672253677));
#37532=CARTESIAN_POINT('Ctrl Pts',(113.682372786808,-4.79084775166455,336.120605844507));
#37533=CARTESIAN_POINT('Ctrl Pts',(113.674614975286,-4.75591420825975,336.25318119447));
#37534=CARTESIAN_POINT('Ctrl Pts',(113.666863001763,-4.72100695345425,336.385656777277));
#37535=CARTESIAN_POINT('Ctrl Pts',(113.65911102824,-4.68053321007231,336.516775777246));
#37536=CARTESIAN_POINT('Ctrl Pts',(113.651359054717,-4.63462367711408,336.64603962104));
#37537=CARTESIAN_POINT('Ctrl Pts',(113.643610364159,-4.58873358687026,336.77524872152));
#37538=CARTESIAN_POINT('Ctrl Pts',(113.635861673602,-4.53741241623104,336.902603860881));
#37539=CARTESIAN_POINT('Ctrl Pts',(113.628112983044,-4.48084068598308,337.027621712583));
#37540=CARTESIAN_POINT('Ctrl Pts',(113.620365904666,-4.42428072595613,337.152613553277));
#37541=CARTESIAN_POINT('Ctrl Pts',(113.612618826288,-4.36247254026919,337.275268717693));
#37542=CARTESIAN_POINT('Ctrl Pts',(113.60487174791,-4.29564460075782,337.395124323805));
#37543=CARTESIAN_POINT('Ctrl Pts',(113.597124604605,-4.22881610116395,337.514980934421));
#37544=CARTESIAN_POINT('Ctrl Pts',(113.589377461299,-4.15696795418387,337.632037598542));
#37545=CARTESIAN_POINT('Ctrl Pts',(113.581630317993,-4.08037415779872,337.745856841656));
#37546=CARTESIAN_POINT('Ctrl Pts',(113.573881432965,-4.00376314150208,337.859701673752));
#37547=CARTESIAN_POINT('Ctrl Pts',(113.566132547937,-3.92240457092562,337.9703073123));
#37548=CARTESIAN_POINT('Ctrl Pts',(113.558383662909,-3.83661501983729,338.077266360272));
#37549=CARTESIAN_POINT('Ctrl Pts',(113.550626553134,-3.75073441083301,338.184338935682));
#37550=CARTESIAN_POINT('Ctrl Pts',(113.542869443359,-3.66041367140612,338.287756883379));
#37551=CARTESIAN_POINT('Ctrl Pts',(113.535112333584,-3.56600918400808,338.387146522085));
#37552=CARTESIAN_POINT('Ctrl Pts',(113.527351078658,-3.47155424987037,338.486589271435));
#37553=CARTESIAN_POINT('Ctrl Pts',(113.519589823732,-3.37301150015818,338.581999150794));
#37554=CARTESIAN_POINT('Ctrl Pts',(113.511828568806,-3.27077250175421,338.673041015871));
#37555=CARTESIAN_POINT('Ctrl Pts',(113.504054898401,-3.16836995427248,338.764228518261));
#37556=CARTESIAN_POINT('Ctrl Pts',(113.496281227997,-3.06225964528318,338.851033795849));
#37557=CARTESIAN_POINT('Ctrl Pts',(113.488507557592,-2.95286508399031,338.933162958517));
#37558=CARTESIAN_POINT('Ctrl Pts',(113.481095753415,-2.84856286584562,339.011468988903));
#37559=CARTESIAN_POINT('Ctrl Pts',(113.473683949238,-2.74127551511268,339.085524289983));
#37560=CARTESIAN_POINT('Ctrl Pts',(113.466272145061,-2.63139129566544,339.155112863882));
#37561=CARTESIAN_POINT('Ctrl Pts',(113.458497066283,-2.51612132329367,339.228112181081));
#37562=CARTESIAN_POINT('Ctrl Pts',(113.450721987504,-2.39762921068808,339.296426536042));
#37563=CARTESIAN_POINT('Ctrl Pts',(113.442946908726,-2.27633272511975,339.359758294567));
#37564=CARTESIAN_POINT('Ctrl Pts',(113.435181397677,-2.15518550259894,339.423012119332));
#37565=CARTESIAN_POINT('Ctrl Pts',(113.427415886628,-2.0312411167115,339.481295368214));
#37566=CARTESIAN_POINT('Ctrl Pts',(113.419650375579,-1.90494619504383,339.534353653663));
#37567=CARTESIAN_POINT('Ctrl Pts',(113.411892564056,-1.77877649515877,339.587359331668));
#37568=CARTESIAN_POINT('Ctrl Pts',(113.404134752534,-1.65026125548881,339.635150205442));
#37569=CARTESIAN_POINT('Ctrl Pts',(113.396376941012,-1.51987127051161,339.677517972555));
#37570=CARTESIAN_POINT('Ctrl Pts',(113.388624967489,-1.38957940813319,339.71985385658));
#37571=CARTESIAN_POINT('Ctrl Pts',(113.380872993966,-1.25741597883199,339.75677463679));
#37572=CARTESIAN_POINT('Ctrl Pts',(113.373121020443,-1.12387097229015,339.788120414123));
#37573=CARTESIAN_POINT('Ctrl Pts',(113.365372329885,-0.990382522137781,
339.819452916501));
#37574=CARTESIAN_POINT('Ctrl Pts',(113.357623639328,-0.855514038205416,
339.845215022766));
#37575=CARTESIAN_POINT('Ctrl Pts',(113.34987494877,-0.719769650248154,339.865296980975));
#37576=CARTESIAN_POINT('Ctrl Pts',(113.342127870392,-0.584053505044566,
339.885374760964));
#37577=CARTESIAN_POINT('Ctrl Pts',(113.334380792014,-0.44746220472576,339.899774686417));
#37578=CARTESIAN_POINT('Ctrl Pts',(113.326633713637,-0.310508635883616,
339.908438392151));
#37579=CARTESIAN_POINT('Ctrl Pts',(113.318886570331,-0.173553919238654,
339.917102170495));
#37580=CARTESIAN_POINT('Ctrl Pts',(113.311139427025,-0.0362373181090265,
339.920029608552));
#37581=CARTESIAN_POINT('Ctrl Pts',(113.303392283719,0.10092500982788,339.91721437451));
#37582=CARTESIAN_POINT('Ctrl Pts',(113.295643398691,0.238118174767959,339.914398507545));
#37583=CARTESIAN_POINT('Ctrl Pts',(113.287894513663,0.375156606782635,339.905837407406));
#37584=CARTESIAN_POINT('Ctrl Pts',(113.280145628635,0.511526400790512,339.891576821823));
#37585=CARTESIAN_POINT('Ctrl Pts',(113.27238851886,0.648040939106898,339.877301099907));
#37586=CARTESIAN_POINT('Ctrl Pts',(113.264631409085,0.783885032357087,339.857313848833));
#37587=CARTESIAN_POINT('Ctrl Pts',(113.256874299311,0.918551584988934,339.831712537829));
#37588=CARTESIAN_POINT('Ctrl Pts',(113.249113044385,1.05329009912071,339.806097546303));
#37589=CARTESIAN_POINT('Ctrl Pts',(113.241351789458,1.1868494384051,339.774862606091));
#37590=CARTESIAN_POINT('Ctrl Pts',(113.233590534532,1.31873587354948,339.738155628334));
#37591=CARTESIAN_POINT('Ctrl Pts',(113.225816864128,1.45083328400832,339.701389931375));
#37592=CARTESIAN_POINT('Ctrl Pts',(113.218043193723,1.581252070644,339.659134825371));
#37593=CARTESIAN_POINT('Ctrl Pts',(113.210269523318,1.70951590985447,339.61158740744));
#37594=CARTESIAN_POINT('Ctrl Pts',(113.202857719141,1.83180903649128,339.566253333252));
#37595=CARTESIAN_POINT('Ctrl Pts',(113.195445914964,1.95214306070018,339.516108683852));
#37596=CARTESIAN_POINT('Ctrl Pts',(113.188034110787,2.0701262333978,339.461363069769));
#37597=CARTESIAN_POINT('Ctrl Pts',(113.180259032009,2.19389211284315,339.403934210061));
#37598=CARTESIAN_POINT('Ctrl Pts',(113.17248395323,2.31546199255914,339.341260481999));
#37599=CARTESIAN_POINT('Ctrl Pts',(113.164708874452,2.43435950775904,339.273532128051));
#37600=CARTESIAN_POINT('Ctrl Pts',(113.156943363403,2.55311071199701,339.205887118154));
#37601=CARTESIAN_POINT('Ctrl Pts',(113.149177852354,2.66919575853113,339.133200050086));
#37602=CARTESIAN_POINT('Ctrl Pts',(113.141412341305,2.78215903162971,339.055708838812));
#37603=CARTESIAN_POINT('Ctrl Pts',(113.133654529782,2.8950103013142,338.9782944603));
#37604=CARTESIAN_POINT('Ctrl Pts',(113.12589671826,3.00474563703244,338.896085637548));
#37605=CARTESIAN_POINT('Ctrl Pts',(113.118138906738,3.11093509892163,338.809365547279));
#37606=CARTESIAN_POINT('Ctrl Pts',(113.110386933215,3.21704464987322,338.722710716628));
#37607=CARTESIAN_POINT('Ctrl Pts',(113.102634959692,3.31961333675318,338.631551622032));
#37608=CARTESIAN_POINT('Ctrl Pts',(113.094882986169,3.41824153549645,338.536213775708));
#37609=CARTESIAN_POINT('Ctrl Pts',(113.087134295611,3.51682796513898,338.440916305019));
#37610=CARTESIAN_POINT('Ctrl Pts',(113.079385605054,3.61147694531549,338.341443873517));
#37611=CARTESIAN_POINT('Ctrl Pts',(113.071636914496,3.70182336973774,338.238161021593));
#37612=CARTESIAN_POINT('Ctrl Pts',(113.063889836118,3.79215099683179,338.134899658529));
#37613=CARTESIAN_POINT('Ctrl Pts',(113.05614275774,3.87817759156433,338.027829745974));
#37614=CARTESIAN_POINT('Ctrl Pts',(113.048395679363,3.95957652104232,337.917350996454));
#37615=CARTESIAN_POINT('Ctrl Pts',(113.040648536057,4.04097613272173,337.806871321016));
#37616=CARTESIAN_POINT('Ctrl Pts',(113.032901392751,4.11774776993411,337.692983066313));
#37617=CARTESIAN_POINT('Ctrl Pts',(113.025154249445,4.18960678558787,337.576116853843));
#37618=CARTESIAN_POINT('Ctrl Pts',(113.017405364417,4.26148195667391,337.459224367368));
#37619=CARTESIAN_POINT('Ctrl Pts',(113.009656479389,4.32844210375113,337.339352923779));
#37620=CARTESIAN_POINT('Ctrl Pts',(113.001907594361,4.39024759353263,337.216959433544));
#37621=CARTESIAN_POINT('Ctrl Pts',(112.994150484586,4.4521186842996,337.094436033594));
#37622=CARTESIAN_POINT('Ctrl Pts',(112.986393374811,4.50882401205307,336.96938558905));
#37623=CARTESIAN_POINT('Ctrl Pts',(112.978636265037,4.56017112224367,336.842287273569));
#37624=CARTESIAN_POINT('Ctrl Pts',(112.970875010111,4.61154567068816,336.715121040813));
#37625=CARTESIAN_POINT('Ctrl Pts',(112.963113755184,4.65755616521626,336.585905124636));
#37626=CARTESIAN_POINT('Ctrl Pts',(112.955352500258,4.69805980220984,336.455134755739));
#37627=CARTESIAN_POINT('Ctrl Pts',(112.947578829854,4.7386282318225,336.32415519687));
#37628=CARTESIAN_POINT('Ctrl Pts',(112.939805159449,4.77367210058735,336.191616594369));
#37629=CARTESIAN_POINT('Ctrl Pts',(112.932031489044,4.80309938564335,336.058026159475));
#37630=CARTESIAN_POINT('Ctrl Pts',(112.924619684867,4.8311568235,335.930654391466));
#37631=CARTESIAN_POINT('Ctrl Pts',(112.91720788069,4.85410876329437,335.802326796206));
#37632=CARTESIAN_POINT('Ctrl Pts',(112.909796076513,4.8719194730853,335.673486236142));
#37633=CARTESIAN_POINT('Ctrl Pts',(112.902020997735,4.89060313881857,335.538330816432));
#37634=CARTESIAN_POINT('Ctrl Pts',(112.894245918956,4.90368790139807,335.402183760527));
#37635=CARTESIAN_POINT('Ctrl Pts',(112.886470840178,4.91107595145501,335.265548604855));
#37636=CARTESIAN_POINT('Ctrl Pts',(112.878705329129,4.91845491004601,335.12908158744));
#37637=CARTESIAN_POINT('Ctrl Pts',(112.87093981808,4.92015108343508,334.992128051929));
#37638=CARTESIAN_POINT('Ctrl Pts',(112.863174307031,4.91611797957733,334.85519988475));
#37639=CARTESIAN_POINT('Ctrl Pts',(112.855416495509,4.9120888745538,334.718407482247));
#37640=CARTESIAN_POINT('Ctrl Pts',(112.847658683986,4.90234180842258,334.581640786208));
#37641=CARTESIAN_POINT('Ctrl Pts',(112.839900872464,4.88688224540193,334.445414585411));
#37642=CARTESIAN_POINT('Ctrl Pts',(112.832148898941,4.87143431619271,334.309290899149));
#37643=CARTESIAN_POINT('Ctrl Pts',(112.824396925418,4.85028249061291,334.173707285351));
#37644=CARTESIAN_POINT('Ctrl Pts',(112.816644951895,4.82348423932062,334.039175949757));
#37645=CARTESIAN_POINT('Ctrl Pts',(112.808896261338,4.79669733710367,333.904701588264));
#37646=CARTESIAN_POINT('Ctrl Pts',(112.80114757078,4.76426884143297,333.771279001173));
#37647=CARTESIAN_POINT('Ctrl Pts',(112.793398880222,4.72630772213892,333.639412487875));
#37648=CARTESIAN_POINT('Ctrl Pts',(112.785651801844,4.6883545009728,333.507573410507));
#37649=CARTESIAN_POINT('Ctrl Pts',(112.777904723467,4.64487105388345,333.377290138345));
#37650=CARTESIAN_POINT('Ctrl Pts',(112.770157645089,4.59601674786154,333.249053651343));
#37651=CARTESIAN_POINT('Ctrl Pts',(112.762410501783,4.54716203239348,333.120816089595));
#37652=CARTESIAN_POINT('Ctrl Pts',(112.754663358477,4.49293650736629,332.994625712486));
#37653=CARTESIAN_POINT('Ctrl Pts',(112.746916215171,4.43354825270876,332.870954919828));
#37654=CARTESIAN_POINT('Ctrl Pts',(112.739167330143,4.37414664631077,332.747256323351));
#37655=CARTESIAN_POINT('Ctrl Pts',(112.731418445115,4.30958016980779,332.626078790794));
#37656=CARTESIAN_POINT('Ctrl Pts',(112.723669560087,4.24010336963785,332.507871095371));
#37657=CARTESIAN_POINT('Ctrl Pts',(112.715912450312,4.17055282607434,332.389537933079));
#37658=CARTESIAN_POINT('Ctrl Pts',(112.708155340538,4.09608174602097,332.27418124228));
#37659=CARTESIAN_POINT('Ctrl Pts',(112.700398230763,4.01698892863049,332.162222170472));
#37660=CARTESIAN_POINT('Ctrl Pts',(112.692636975837,3.93785384656735,332.050203271316));
#37661=CARTESIAN_POINT('Ctrl Pts',(112.68487572091,3.85409234462456,331.941585918225));
#37662=CARTESIAN_POINT('Ctrl Pts',(112.677114465984,3.7660435936311,331.836758195558));
#37663=CARTESIAN_POINT('Ctrl Pts',(112.66934079558,3.67785399333106,331.731762782697));
#37664=CARTESIAN_POINT('Ctrl Pts',(112.661567125175,3.58536370310621,331.630569402948));
#37665=CARTESIAN_POINT('Ctrl Pts',(112.65379345477,3.48894944885784,331.533529921402));
#37666=CARTESIAN_POINT('Ctrl Pts',(112.646381650593,3.39702330134008,331.441007651068));
#37667=CARTESIAN_POINT('Ctrl Pts',(112.638969846416,3.30153050034026,331.352261450004));
#37668=CARTESIAN_POINT('Ctrl Pts',(112.631558042239,3.20282412173445,331.267561024245));
#37669=CARTESIAN_POINT('Ctrl Pts',(112.62378296346,3.09927984948263,331.17870917831));
#37670=CARTESIAN_POINT('Ctrl Pts',(112.616007884682,2.99187180143713,331.094028938239));
#37671=CARTESIAN_POINT('Ctrl Pts',(112.608232805904,2.88097048186124,331.013875046471));
#37672=CARTESIAN_POINT('Ctrl Pts',(112.600467294855,2.77020563341941,330.93381978917));
#37673=CARTESIAN_POINT('Ctrl Pts',(112.592701783806,2.65595638037961,330.858280024324));
#37674=CARTESIAN_POINT('Ctrl Pts',(112.584936272757,2.53862801944713,330.787571859203));
#37675=CARTESIAN_POINT('Ctrl Pts',(112.577178461234,2.42141598992611,330.716933801434));
#37676=CARTESIAN_POINT('Ctrl Pts',(112.569420649712,2.30113126066751,330.65111801039));
#37677=CARTESIAN_POINT('Ctrl Pts',(112.56166283819,2.17820968553823,330.59039847284));
#37678=CARTESIAN_POINT('Ctrl Pts',(112.553910864667,2.05538061279238,330.529724628668));
#37679=CARTESIAN_POINT('Ctrl Pts',(112.546158891144,1.92991899288691,330.47413957684));
#37680=CARTESIAN_POINT('Ctrl Pts',(112.538406917621,1.8022866512284,330.423872172972));
#37681=CARTESIAN_POINT('Ctrl Pts',(112.530658227063,1.67470836194228,330.373626057378));
#37682=CARTESIAN_POINT('Ctrl Pts',(112.522909536506,1.54496154225741,330.328693253558));
#37683=CARTESIAN_POINT('Ctrl Pts',(112.515160845948,1.41352923811787,330.289255031793));
#37684=CARTESIAN_POINT('Ctrl Pts',(112.50741376757,1.28212427956694,330.24982501548));
#37685=CARTESIAN_POINT('Ctrl Pts',(112.499666689192,1.14903490823484,330.215887419597));
#37686=CARTESIAN_POINT('Ctrl Pts',(112.491919610814,1.01476024226081,330.187573926466));
#37687=CARTESIAN_POINT('Ctrl Pts',(112.484172467509,0.880484450935939,330.159260196042));
#37688=CARTESIAN_POINT('Ctrl Pts',(112.476425324203,0.745023727619236,330.136570743032));
#37689=CARTESIAN_POINT('Ctrl Pts',(112.468678180897,0.608887927380469,330.119586231231));
#37690=CARTESIAN_POINT('Ctrl Pts',(112.460929295869,0.472721520923564,330.102597900951));
#37691=CARTESIAN_POINT('Ctrl Pts',(112.453180410841,0.335880123327505,330.091317112476));
#37692=CARTESIAN_POINT('Ctrl Pts',(112.445431525813,0.198878867246145,330.085772669212));
#37693=CARTESIAN_POINT('Ctrl Pts',(112.437674416038,0.0617321966159992,
330.080222341019));
#37694=CARTESIAN_POINT('Ctrl Pts',(112.429917306263,-0.0755742802706099,
330.08042053645));
#37695=CARTESIAN_POINT('Ctrl Pts',(112.422160196489,-0.212524714131034,
330.086343895999));
#37696=CARTESIAN_POINT('Ctrl Pts',(112.414398941562,-0.349548329924487,
330.092270420803));
#37697=CARTESIAN_POINT('Ctrl Pts',(112.406637686636,-0.486215134323129,
330.10392817254));
#37698=CARTESIAN_POINT('Ctrl Pts',(112.39887643171,-0.622015234114492,330.12124194994));
#37699=CARTESIAN_POINT('Ctrl Pts',(112.391102761305,-0.758032569808371,
330.13858342374));
#37700=CARTESIAN_POINT('Ctrl Pts',(112.383329090901,-0.893180044838139,
330.161598937727));
#37701=CARTESIAN_POINT('Ctrl Pts',(112.375555420496,-1.02695790033932,330.190162109444));
#37702=CARTESIAN_POINT('Ctrl Pts',(112.368143616319,-1.15450836448048,330.217395658645));
#37703=CARTESIAN_POINT('Ctrl Pts',(112.360731812142,-1.2808135722666,330.249671930603));
#37704=CARTESIAN_POINT('Ctrl Pts',(112.353320007965,-1.40545565252448,330.286839969693));
#37705=CARTESIAN_POINT('Ctrl Pts',(112.345544929187,-1.53620681242671,330.325829725096));
#37706=CARTESIAN_POINT('Ctrl Pts',(112.337769850408,-1.66554089074588,330.370326107294));
#37707=CARTESIAN_POINT('Ctrl Pts',(112.32999477163,-1.79295907588046,330.420209522836));
#37708=CARTESIAN_POINT('Ctrl Pts',(112.322229260581,-1.92022046482639,330.47003155366));
#37709=CARTESIAN_POINT('Ctrl Pts',(112.314463749532,-2.0455702910965,330.525227286713));
#37710=CARTESIAN_POINT('Ctrl Pts',(112.306698238483,-2.1685234040396,330.585626963131));
#37711=CARTESIAN_POINT('Ctrl Pts',(112.29894042696,-2.29135460861308,330.645966753095));
#37712=CARTESIAN_POINT('Ctrl Pts',(112.291182615438,-2.41179348035784,330.711500047047));
#37713=CARTESIAN_POINT('Ctrl Pts',(112.283424803916,-2.52937375241882,330.782008596135));
#37714=CARTESIAN_POINT('Ctrl Pts',(112.275672830393,-2.64686554159646,330.852464085305));
#37715=CARTESIAN_POINT('Ctrl Pts',(112.26792085687,-2.76150267905072,330.927887177076));
#37716=CARTESIAN_POINT('Ctrl Pts',(112.260168883347,-2.87284279498562,331.008013359516));
#37717=CARTESIAN_POINT('Ctrl Pts',(112.252420192789,-2.98413575831538,331.088105608471));
#37718=CARTESIAN_POINT('Ctrl Pts',(112.244671502232,-3.09213416064943,331.172896758781));
#37719=CARTESIAN_POINT('Ctrl Pts',(112.236922811674,-3.19642416406312,331.262078702555));
#37720=CARTESIAN_POINT('Ctrl Pts',(112.229175733296,-3.3006924690705,331.351242091281));
#37721=CARTESIAN_POINT('Ctrl Pts',(112.221428654918,-3.40125361296962,331.4447942025));
#37722=CARTESIAN_POINT('Ctrl Pts',(112.213681576541,-3.49772675982205,331.542386577981));
#37723=CARTESIAN_POINT('Ctrl Pts',(112.205934433235,-3.59420071521237,331.63997977138));
#37724=CARTESIAN_POINT('Ctrl Pts',(112.198187289929,-3.68658633042788,331.741613018601));
#37725=CARTESIAN_POINT('Ctrl Pts',(112.190440146623,-3.77453986172993,331.846901223445));
#37726=CARTESIAN_POINT('Ctrl Pts',(112.182691261595,-3.86251316685307,331.952213099313));
#37727=CARTESIAN_POINT('Ctrl Pts',(112.174942376567,-3.94605215474399,332.061181267999));
#37728=CARTESIAN_POINT('Ctrl Pts',(112.167193491539,-4.02485383616609,332.173388130641));
#37729=CARTESIAN_POINT('Ctrl Pts',(112.159436381764,-4.10373915850704,332.285714090807));
#37730=CARTESIAN_POINT('Ctrl Pts',(112.151679271989,-4.17787690502825,332.401285291446));
#37731=CARTESIAN_POINT('Ctrl Pts',(112.143922162215,-4.24700756358994,332.519655302723));
#37732=CARTESIAN_POINT('Ctrl Pts',(112.136160907288,-4.31617516336514,332.638088567149));
#37733=CARTESIAN_POINT('Ctrl Pts',(112.128399652362,-4.38033016102159,332.759323277013));
#37734=CARTESIAN_POINT('Ctrl Pts',(112.120638397436,-4.43925986243837,332.882889956511));
#37735=CARTESIAN_POINT('Ctrl Pts',(112.112864727032,-4.49828383217231,333.006654302425));
#37736=CARTESIAN_POINT('Ctrl Pts',(112.105091056627,-4.55206564894555,333.132757712671));
#37737=CARTESIAN_POINT('Ctrl Pts',(112.097317386222,-4.60044114226395,333.260711536557));
#37738=CARTESIAN_POINT('Ctrl Pts',(112.089905582045,-4.64656474473003,333.382709079158));
#37739=CARTESIAN_POINT('Ctrl Pts',(112.082493777868,-4.68777393438105,333.506388365759));
#37740=CARTESIAN_POINT('Ctrl Pts',(112.075081973691,-4.72396951895452,333.631316308825));
#37741=CARTESIAN_POINT('Ctrl Pts',(112.065386055773,-4.77131958496133,333.794743600301));
#37742=CARTESIAN_POINT('Ctrl Pts',(112.055690137855,-4.8102122349805,333.960723810202));
#37743=CARTESIAN_POINT('Ctrl Pts',(112.045994219937,-4.84041651357817,334.128477746939));
#37744=CARTESIAN_POINT('Ctrl Pts',(112.036441766059,-4.87017387958176,334.2937495404));
#37745=CARTESIAN_POINT('Ctrl Pts',(112.026889312181,-4.89149809061967,334.460743035106));
#37746=CARTESIAN_POINT('Ctrl Pts',(112.017336858303,-4.90421385269992,334.628692109583));
#37747=CARTESIAN_POINT('Ctrl Pts',(112.010403321699,-4.91344343945979,334.750595975379));
#37748=CARTESIAN_POINT('Ctrl Pts',(112.003469785094,-4.91813866033305,334.873002852249));
#37749=CARTESIAN_POINT('Ctrl Pts',(111.99653624849,-4.91824804283262,334.995612327148));
#37750=CARTESIAN_POINT('',(115.496536248451,-4.91824814755885,335.004268668875));
#37751=CARTESIAN_POINT('Ctrl Pts',(115.496536248451,-4.91824814755885,335.004268668875));
#37752=CARTESIAN_POINT('Ctrl Pts',(115.48716948192,-4.91810431769546,335.169985659309));
#37753=CARTESIAN_POINT('Ctrl Pts',(115.477802715389,-4.90958118452984,335.335335957126));
#37754=CARTESIAN_POINT('Ctrl Pts',(115.468435948858,-4.89281220431308,335.499571612309));
#37755=CARTESIAN_POINT('Ctrl Pts',(115.458942508385,-4.87581644436368,335.66602835175));
#37756=CARTESIAN_POINT('Ctrl Pts',(115.449449067914,-4.85035035781784,335.831340101219));
#37757=CARTESIAN_POINT('Ctrl Pts',(115.439955627442,-4.8166019771811,335.994750449065));
#37758=CARTESIAN_POINT('Ctrl Pts',(115.431283213287,-4.78577227589518,336.144028491924));
#37759=CARTESIAN_POINT('Ctrl Pts',(115.422610799133,-4.74803152286972,336.291720084277));
#37760=CARTESIAN_POINT('Ctrl Pts',(115.413938384978,-4.70355762201091,336.437264331612));
#37761=CARTESIAN_POINT('Ctrl Pts',(115.4061633062,-4.66368543917903,336.567749104204));
#37762=CARTESIAN_POINT('Ctrl Pts',(115.398388227421,-4.61831632860917,336.696779626366));
#37763=CARTESIAN_POINT('Ctrl Pts',(115.390613148643,-4.56757325085014,336.823857905819));
#37764=CARTESIAN_POINT('Ctrl Pts',(115.382847637594,-4.51689261567874,336.950779807359));
#37765=CARTESIAN_POINT('Ctrl Pts',(115.375082126545,-4.46085131487353,337.07575388666));
#37766=CARTESIAN_POINT('Ctrl Pts',(115.367316615496,-4.39962238096218,337.198296150985));
#37767=CARTESIAN_POINT('Ctrl Pts',(115.359558803974,-4.33845415571703,337.320716914299));
#37768=CARTESIAN_POINT('Ctrl Pts',(115.351800992452,-4.27210870691022,337.440710313559));
#37769=CARTESIAN_POINT('Ctrl Pts',(115.344043180929,-4.20080742837961,337.557811566979));
#37770=CARTESIAN_POINT('Ctrl Pts',(115.336291207406,-4.12955980632228,337.674824697992));
#37771=CARTESIAN_POINT('Ctrl Pts',(115.328539233883,-4.05336398022909,337.788949682732));
#37772=CARTESIAN_POINT('Ctrl Pts',(115.32078726036,-3.97248744451886,337.899745948465));
#37773=CARTESIAN_POINT('Ctrl Pts',(115.313038569803,-3.89164516006953,338.010495291914));
#37774=CARTESIAN_POINT('Ctrl Pts',(115.305289879245,-3.80612633860054,338.117918405125));
#37775=CARTESIAN_POINT('Ctrl Pts',(115.297541188688,-3.71624187673964,338.221603541106));
#37776=CARTESIAN_POINT('Ctrl Pts',(115.28979411031,-3.62637611609182,338.325267104528));
#37777=CARTESIAN_POINT('Ctrl Pts',(115.282047031932,-3.53214677761466,338.425193942495));
#37778=CARTESIAN_POINT('Ctrl Pts',(115.274299953554,-3.4339048844054,338.521005581841));
#37779=CARTESIAN_POINT('Ctrl Pts',(115.266552810248,-3.33566216783445,338.616818024181));
#37780=CARTESIAN_POINT('Ctrl Pts',(115.258805666943,-3.233407109285,338.708514926203));
#37781=CARTESIAN_POINT('Ctrl Pts',(115.251058523637,-3.12752711840107,338.795755153611));
#37782=CARTESIAN_POINT('Ctrl Pts',(115.243309638609,-3.02162332344737,338.883014994474));
#37783=CARTESIAN_POINT('Ctrl Pts',(115.235560753581,-2.91209327608224,338.965815918435));
#37784=CARTESIAN_POINT('Ctrl Pts',(115.227811868553,-2.7993566125464,339.04385776435));
#37785=CARTESIAN_POINT('Ctrl Pts',(115.220054758778,-2.68650028915093,339.121982444686));
#37786=CARTESIAN_POINT('Ctrl Pts',(115.212297649003,-2.57043087259344,339.195337733633));
#37787=CARTESIAN_POINT('Ctrl Pts',(115.204540539228,-2.45159653571134,339.263667140923));
#37788=CARTESIAN_POINT('Ctrl Pts',(115.196779284302,-2.3326986975592,339.332033061264));
#37789=CARTESIAN_POINT('Ctrl Pts',(115.189018029376,-2.21103334159486,339.395367568116));
#37790=CARTESIAN_POINT('Ctrl Pts',(115.18125677445,-2.08707136980889,339.453461143855));
#37791=CARTESIAN_POINT('Ctrl Pts',(115.173483104045,-1.96291109926726,339.511647650382));
#37792=CARTESIAN_POINT('Ctrl Pts',(115.165709433641,-1.83644723224796,339.56457632153));
#37793=CARTESIAN_POINT('Ctrl Pts',(115.157935763236,-1.70816951737834,339.612086291734));
#37794=CARTESIAN_POINT('Ctrl Pts',(115.150523959059,-1.58586316099757,339.657384661395));
#37795=CARTESIAN_POINT('Ctrl Pts',(115.143112154882,-1.4619082993518,339.69775736901));
#37796=CARTESIAN_POINT('Ctrl Pts',(115.135700350705,-1.33673868020804,339.733108150395));
#37797=CARTESIAN_POINT('Ctrl Pts',(115.127925271926,-1.20543412516908,339.77019157888));
#37798=CARTESIAN_POINT('Ctrl Pts',(115.120150193148,-1.07237777732891,339.801865545206));
#37799=CARTESIAN_POINT('Ctrl Pts',(115.11237511437,-0.938054950028191,339.827963957325));
#37800=CARTESIAN_POINT('Ctrl Pts',(115.104609603321,-0.803897415517961,
339.854030253686));
#37801=CARTESIAN_POINT('Ctrl Pts',(115.096844092272,-0.668476882513542,
339.874534573571));
#37802=CARTESIAN_POINT('Ctrl Pts',(115.089078581223,-0.5322939886632,339.889360507483));
#37803=CARTESIAN_POINT('Ctrl Pts',(115.0813207697,-0.396246120548597,339.904171741438));
#37804=CARTESIAN_POINT('Ctrl Pts',(115.073562958178,-0.259437781913177,
339.913315751678));
#37805=CARTESIAN_POINT('Ctrl Pts',(115.065805146656,-0.122379626587724,
339.91672719291));
#37806=CARTESIAN_POINT('Ctrl Pts',(115.058053173133,0.0145753881293899,
339.920136066923));
#37807=CARTESIAN_POINT('Ctrl Pts',(115.05030119961,0.151779456161817,339.917820948928));
#37808=CARTESIAN_POINT('Ctrl Pts',(115.042549226087,0.288717333918926,339.909768361501));
#37809=CARTESIAN_POINT('Ctrl Pts',(115.034800535529,0.425597218403598,339.901719184349));
#37810=CARTESIAN_POINT('Ctrl Pts',(115.027051844972,0.562210747440298,339.887937393407));
#37811=CARTESIAN_POINT('Ctrl Pts',(115.019303154414,0.698043430194164,339.868461608359));
#37812=CARTESIAN_POINT('Ctrl Pts',(115.011556076036,0.833847851823886,339.84898987541));
#37813=CARTESIAN_POINT('Ctrl Pts',(115.003808997659,0.968871363643894,339.823826560214));
#37814=CARTESIAN_POINT('Ctrl Pts',(114.996061919281,1.10260574075635,339.793062032037));
#37815=CARTESIAN_POINT('Ctrl Pts',(114.988314775975,1.23634123869161,339.762297246023));
#37816=CARTESIAN_POINT('Ctrl Pts',(114.980567632669,1.36878719944449,339.725931241024));
#37817=CARTESIAN_POINT('Ctrl Pts',(114.972820489363,1.49944710632027,339.684105190733));
#37818=CARTESIAN_POINT('Ctrl Pts',(114.965071604335,1.63013638831711,339.642269737057));
#37819=CARTESIAN_POINT('Ctrl Pts',(114.957322719307,1.75903844521842,339.594971914578));
#37820=CARTESIAN_POINT('Ctrl Pts',(114.949573834279,1.8856737758654,339.542402169944));
#37821=CARTESIAN_POINT('Ctrl Pts',(114.941816724504,2.01244351856081,339.48977662724));
#37822=CARTESIAN_POINT('Ctrl Pts',(114.93405961473,2.13694136736339,339.431868134599));
#37823=CARTESIAN_POINT('Ctrl Pts',(114.926302504955,2.25870910209775,339.368914768521));
#37824=CARTESIAN_POINT('Ctrl Pts',(114.918541250029,2.3805419056161,339.305927762177));
#37825=CARTESIAN_POINT('Ctrl Pts',(114.910779995102,2.49964134887912,339.237890704521));
#37826=CARTESIAN_POINT('Ctrl Pts',(114.903018740176,2.61557641195957,339.165086205074));
#37827=CARTESIAN_POINT('Ctrl Pts',(114.895245069772,2.73169693335781,339.092165242156));
#37828=CARTESIAN_POINT('Ctrl Pts',(114.887471399367,2.84464263704903,339.014461819395));
#37829=CARTESIAN_POINT('Ctrl Pts',(114.879697728962,2.95401321666414,338.932300723276));
#37830=CARTESIAN_POINT('Ctrl Pts',(114.872285924785,3.0582925694855,338.853964245947));
#37831=CARTESIAN_POINT('Ctrl Pts',(114.864874120608,3.15932192879822,338.771575947004));
#37832=CARTESIAN_POINT('Ctrl Pts',(114.857462316431,3.25678561819087,338.685448480124));
#37833=CARTESIAN_POINT('Ctrl Pts',(114.849687237653,3.35902629332978,338.595099649532));
#37834=CARTESIAN_POINT('Ctrl Pts',(114.841912158874,3.45766603193587,338.500350328631));
#37835=CARTESIAN_POINT('Ctrl Pts',(114.834137080096,3.55230253276615,338.401518745826));
#37836=CARTESIAN_POINT('Ctrl Pts',(114.826371569047,3.64682257735731,338.302808781575));
#37837=CARTESIAN_POINT('Ctrl Pts',(114.818606057998,3.73734891822672,338.200026830329));
#37838=CARTESIAN_POINT('Ctrl Pts',(114.810840546949,3.82351274038597,338.093530893107));
#37839=CARTESIAN_POINT('Ctrl Pts',(114.803082735426,3.90959113086463,337.987140546917));
#37840=CARTESIAN_POINT('Ctrl Pts',(114.795324923904,3.99131536625086,337.877043844904));
#37841=CARTESIAN_POINT('Ctrl Pts',(114.787567112382,4.0683541522042,337.763634844682));
#37842=CARTESIAN_POINT('Ctrl Pts',(114.779815138859,4.14533496402801,337.65031118833));
#37843=CARTESIAN_POINT('Ctrl Pts',(114.772063165336,4.21763712589514,337.533680517212));
#37844=CARTESIAN_POINT('Ctrl Pts',(114.764311191813,4.28497047648131,337.41416881725));
#37845=CARTESIAN_POINT('Ctrl Pts',(114.756562501255,4.35227531135357,337.294707730564));
#37846=CARTESIAN_POINT('Ctrl Pts',(114.748813810698,4.41461532877343,337.172368381598));
#37847=CARTESIAN_POINT('Ctrl Pts',(114.74106512014,4.47174458434419,337.047604315997));
#37848=CARTESIAN_POINT('Ctrl Pts',(114.733318041762,4.52886195369618,336.922866208601));
#37849=CARTESIAN_POINT('Ctrl Pts',(114.725570963384,4.58077055500555,336.795704743189));
#37850=CARTESIAN_POINT('Ctrl Pts',(114.717823885007,4.62727135206123,336.666596200912));
#37851=CARTESIAN_POINT('Ctrl Pts',(114.710076741701,4.67377253883835,336.537486576581));
#37852=CARTESIAN_POINT('Ctrl Pts',(114.702329598395,4.71486569851094,336.406430210587));
#37853=CARTESIAN_POINT('Ctrl Pts',(114.694582455089,4.75040085337575,336.273921031598));
#37854=CARTESIAN_POINT('Ctrl Pts',(114.686833570061,4.78594399729778,336.141382061731));
#37855=CARTESIAN_POINT('Ctrl Pts',(114.679084685033,4.8159265487081,336.007390006387));
#37856=CARTESIAN_POINT('Ctrl Pts',(114.671335800005,4.84024917266582,335.872451149926));
#37857=CARTESIAN_POINT('Ctrl Pts',(114.66357869023,4.86459761290791,335.73736906797));
#37858=CARTESIAN_POINT('Ctrl Pts',(114.655821580455,4.88327405569469,335.60133856271));
#37859=CARTESIAN_POINT('Ctrl Pts',(114.648064470681,4.89623073540441,335.464873798123));
#37860=CARTESIAN_POINT('Ctrl Pts',(114.640303215755,4.90919433874949,335.328336111129));
#37861=CARTESIAN_POINT('Ctrl Pts',(114.632541960828,4.9164320681337,335.191364092551));
#37862=CARTESIAN_POINT('Ctrl Pts',(114.624780705902,4.91794832631852,335.054473132468));
#37863=CARTESIAN_POINT('Ctrl Pts',(114.617007035498,4.91946701002228,334.917363191462));
#37864=CARTESIAN_POINT('Ctrl Pts',(114.609233365093,4.91524594518383,334.780334958961));
#37865=CARTESIAN_POINT('Ctrl Pts',(114.601459694688,4.90534162293875,334.64390082173));
#37866=CARTESIAN_POINT('Ctrl Pts',(114.594047890511,4.89589834927706,334.513817726412));
#37867=CARTESIAN_POINT('Ctrl Pts',(114.586636086334,4.88128905440621,334.384274946802));
#37868=CARTESIAN_POINT('Ctrl Pts',(114.579224282157,4.86160582485375,334.255707136775));
#37869=CARTESIAN_POINT('Ctrl Pts',(114.571449203379,4.84095786158752,334.120837835393));
#37870=CARTESIAN_POINT('Ctrl Pts',(114.5636741246,4.81466075876088,333.986615280559));
#37871=CARTESIAN_POINT('Ctrl Pts',(114.555899045822,4.78276441314124,333.853549987618));
#37872=CARTESIAN_POINT('Ctrl Pts',(114.548133534773,4.7509073180055,333.720648439992));
#37873=CARTESIAN_POINT('Ctrl Pts',(114.540368023724,4.71346477989057,333.588901697214));
#37874=CARTESIAN_POINT('Ctrl Pts',(114.532602512675,4.67053826253905,333.45881363857));
#37875=CARTESIAN_POINT('Ctrl Pts',(114.524844701153,4.62765430695445,333.328854562614));
#37876=CARTESIAN_POINT('Ctrl Pts',(114.51708688963,4.57929731452527,333.200551266761));
#37877=CARTESIAN_POINT('Ctrl Pts',(114.509329078108,4.52561937432772,333.074395590676));
#37878=CARTESIAN_POINT('Ctrl Pts',(114.501577104585,4.47198182848235,332.948334850737));
#37879=CARTESIAN_POINT('Ctrl Pts',(114.493825131062,4.41303145741679,332.824418871915));
#37880=CARTESIAN_POINT('Ctrl Pts',(114.486073157539,4.3489694588376,332.703122182484));
#37881=CARTESIAN_POINT('Ctrl Pts',(114.478324466982,4.28493459055289,332.581876862273));
#37882=CARTESIAN_POINT('Ctrl Pts',(114.470575776424,4.21579258250683,332.463248970102));
#37883=CARTESIAN_POINT('Ctrl Pts',(114.462827085866,4.1417917362836,332.347690765436));
#37884=CARTESIAN_POINT('Ctrl Pts',(114.455080007488,4.06780628655445,332.23215660362));
#37885=CARTESIAN_POINT('Ctrl Pts',(114.447332929111,3.9889642201012,332.119691187899));
#37886=CARTESIAN_POINT('Ctrl Pts',(114.439585850733,3.90555834199266,332.010719635131));
#37887=CARTESIAN_POINT('Ctrl Pts',(114.431838707427,3.82215176486263,331.901747169077));
#37888=CARTESIAN_POINT('Ctrl Pts',(114.424091564121,3.73418153735742,331.796268934772));
#37889=CARTESIAN_POINT('Ctrl Pts',(114.416344420815,3.64198185308981,331.694678344811));
#37890=CARTESIAN_POINT('Ctrl Pts',(114.408595535787,3.54976144037567,331.593064915128));
#37891=CARTESIAN_POINT('Ctrl Pts',(114.400846650759,3.45330994140741,331.495341158387));
#37892=CARTESIAN_POINT('Ctrl Pts',(114.393097765731,3.35299934567111,331.40186458698));
#37893=CARTESIAN_POINT('Ctrl Pts',(114.385340655956,3.2525822792321,331.308288798574));
#37894=CARTESIAN_POINT('Ctrl Pts',(114.377583546182,3.14829822012146,331.218969467565));
#37895=CARTESIAN_POINT('Ctrl Pts',(114.369826436407,3.04055369107716,331.134225004714));
#37896=CARTESIAN_POINT('Ctrl Pts',(114.362065181481,2.93275158680162,331.049435257132));
#37897=CARTESIAN_POINT('Ctrl Pts',(114.354303926554,2.8214856448798,330.969225477377));
#37898=CARTESIAN_POINT('Ctrl Pts',(114.346542671628,2.70719165041267,330.893870870219));
#37899=CARTESIAN_POINT('Ctrl Pts',(114.338769001224,2.59271482280271,330.818395720248));
#37900=CARTESIAN_POINT('Ctrl Pts',(114.330995330819,2.47520059833398,330.747791464438));
#37901=CARTESIAN_POINT('Ctrl Pts',(114.323221660414,2.35511042456542,330.682287880068));
#37902=CARTESIAN_POINT('Ctrl Pts',(114.315809856237,2.24061047727715,330.61983350331));
#37903=CARTESIAN_POINT('Ctrl Pts',(114.30839805206,2.12376926249241,330.562015739833));
#37904=CARTESIAN_POINT('Ctrl Pts',(114.300986247883,2.00500212323059,330.508992368261));
#37905=CARTESIAN_POINT('Ctrl Pts',(114.293211169104,1.88041385268503,330.4533701633));
#37906=CARTESIAN_POINT('Ctrl Pts',(114.285436090326,1.7533123715449,330.402848431981));
#37907=CARTESIAN_POINT('Ctrl Pts',(114.277661011548,1.62415398506101,330.357661484197));
#37908=CARTESIAN_POINT('Ctrl Pts',(114.269895500499,1.49515453619431,330.312530141828));
#37909=CARTESIAN_POINT('Ctrl Pts',(114.26212998945,1.36410358367196,330.272720648787));
#37910=CARTESIAN_POINT('Ctrl Pts',(114.254364478401,1.2314797581886,330.238420360041));
#37911=CARTESIAN_POINT('Ctrl Pts',(114.246606666878,1.09898742961442,330.204154080132));
#37912=CARTESIAN_POINT('Ctrl Pts',(114.238848855356,0.964925707573891,330.175386231289));
#37913=CARTESIAN_POINT('Ctrl Pts',(114.231091043834,0.829790494659489,330.152255081229));
#37914=CARTESIAN_POINT('Ctrl Pts',(114.223339070311,0.694756975278188,330.129141338092));
#37915=CARTESIAN_POINT('Ctrl Pts',(114.215587096788,0.558651956700592,330.111655916335));
#37916=CARTESIAN_POINT('Ctrl Pts',(114.207835123265,0.421983359498487,330.099886418989));
#37917=CARTESIAN_POINT('Ctrl Pts',(114.200086432707,0.285372641528438,330.088121906033));
#37918=CARTESIAN_POINT('Ctrl Pts',(114.19233774215,0.148199208265827,330.082068536358));
#37919=CARTESIAN_POINT('Ctrl Pts',(114.184589051592,0.0109777445768436,
330.081762251413));
#37920=CARTESIAN_POINT('Ctrl Pts',(114.176841973214,-0.12621516904043,330.081456030193));
#37921=CARTESIAN_POINT('Ctrl Pts',(114.169094894836,-0.263455702579121,
330.086894516185));
#37922=CARTESIAN_POINT('Ctrl Pts',(114.161347816458,-0.400227912580374,
330.098061538484));
#37923=CARTESIAN_POINT('Ctrl Pts',(114.153600673153,-0.537001268864482,
330.109228654373));
#37924=CARTESIAN_POINT('Ctrl Pts',(114.145853529847,-0.673305904204498,
330.126124370523));
#37925=CARTESIAN_POINT('Ctrl Pts',(114.138106386541,-0.808630138217336,
330.148680554523));
#37926=CARTESIAN_POINT('Ctrl Pts',(114.130357501513,-0.943984795990994,
330.171241809632));
#37927=CARTESIAN_POINT('Ctrl Pts',(114.122608616485,-1.07835822835649,330.199466000656));
#37928=CARTESIAN_POINT('Ctrl Pts',(114.114859731457,-1.21124849066157,330.233233784171));
#37929=CARTESIAN_POINT('Ctrl Pts',(114.107102621682,-1.34427980406407,330.26703740916));
#37930=CARTESIAN_POINT('Ctrl Pts',(114.099345511907,-1.47582442325646,330.306396284118));
#37931=CARTESIAN_POINT('Ctrl Pts',(114.091588402132,-1.60539459705742,330.351140865735));
#37932=CARTESIAN_POINT('Ctrl Pts',(114.083827147206,-1.73503400901633,330.395909357426));
#37933=CARTESIAN_POINT('Ctrl Pts',(114.07606589228,-1.86269650962508,330.446069147481));
#37934=CARTESIAN_POINT('Ctrl Pts',(114.068304637354,-1.98791484499822,330.501402704005));
#37935=CARTESIAN_POINT('Ctrl Pts',(114.060530966949,-2.11333348889947,330.556824776186));
#37936=CARTESIAN_POINT('Ctrl Pts',(114.052757296545,-2.23629980371065,330.617436980507));
#37937=CARTESIAN_POINT('Ctrl Pts',(114.04498362614,-2.35637084906335,330.682975621544));
#37938=CARTESIAN_POINT('Ctrl Pts',(114.037571821963,-2.470852558366,330.745463423072));
#37939=CARTESIAN_POINT('Ctrl Pts',(114.030160017786,-2.58270223482796,330.812429183881));
#37940=CARTESIAN_POINT('Ctrl Pts',(114.022748213609,-2.69156243309646,330.883609016232));
#37941=CARTESIAN_POINT('Ctrl Pts',(114.014983182136,-2.80561062507305,330.958181094127));
#37942=CARTESIAN_POINT('Ctrl Pts',(114.007218150664,-2.91673988008223,331.037615837191));
#37943=CARTESIAN_POINT('Ctrl Pts',(113.999453119191,-3.02450689708768,331.121657429782));
#37944=CARTESIAN_POINT('Ctrl Pts',(113.99169765018,-3.13214120143334,331.205595527039));
#37945=CARTESIAN_POINT('Ctrl Pts',(113.983942181169,-3.23642119965978,331.294128947552));
#37946=CARTESIAN_POINT('Ctrl Pts',(113.976186712158,-3.33693093749876,331.386957655816));
#37947=CARTESIAN_POINT('Ctrl Pts',(113.968438926609,-3.43734109880006,331.479694397257));
#37948=CARTESIAN_POINT('Ctrl Pts',(113.960691141061,-3.53398814660308,331.576717694108));
#37949=CARTESIAN_POINT('Ctrl Pts',(113.952943355512,-3.62648801736549,331.677686390118));
#37950=CARTESIAN_POINT('Ctrl Pts',(113.945201381181,-3.71891850869959,331.778579354667));
#37951=CARTESIAN_POINT('Ctrl Pts',(113.93745940685,-3.80720775043846,331.883411540521));
#37952=CARTESIAN_POINT('Ctrl Pts',(113.92971743252,-3.89100775402714,331.991804241642));
#37953=CARTESIAN_POINT('Ctrl Pts',(113.921978697296,-3.97477269715578,332.100151593148));
#37954=CARTESIAN_POINT('Ctrl Pts',(113.914239962072,-4.05405189823505,332.212056187804));
#37955=CARTESIAN_POINT('Ctrl Pts',(113.906501226849,-4.12853713695404,332.327105656542));
#37956=CARTESIAN_POINT('Ctrl Pts',(113.898764059831,-4.20300728171342,332.442131811236));
#37957=CARTESIAN_POINT('Ctrl Pts',(113.891026892812,-4.27268518341832,332.560301243582));
#37958=CARTESIAN_POINT('Ctrl Pts',(113.883289725794,-4.33730575999222,332.681172320581));
#37959=CARTESIAN_POINT('Ctrl Pts',(113.875552440266,-4.40192732635598,332.802045248957));
#37960=CARTESIAN_POINT('Ctrl Pts',(113.867815154738,-4.4614912284773,332.925619558689));
#37961=CARTESIAN_POINT('Ctrl Pts',(113.860077869211,-4.51577839106033,333.051429091531));
#37962=CARTESIAN_POINT('Ctrl Pts',(113.85233877873,-4.57007821774068,333.177267973193));
#37963=CARTESIAN_POINT('Ctrl Pts',(113.84459968825,-4.61909870032521,333.305342755621));
#37964=CARTESIAN_POINT('Ctrl Pts',(113.83686059777,-4.66266910488782,333.435167778698));
#37965=CARTESIAN_POINT('Ctrl Pts',(113.829113285313,-4.70628579846462,333.565130727332));
#37966=CARTESIAN_POINT('Ctrl Pts',(113.821365972855,-4.74444072371911,333.69684725854));
#37967=CARTESIAN_POINT('Ctrl Pts',(113.813618660398,-4.77701305493719,333.829816537692));
#37968=CARTESIAN_POINT('Ctrl Pts',(113.805867127408,-4.8096031307091,333.962858255028));
#37969=CARTESIAN_POINT('Ctrl Pts',(113.798115594417,-4.83660447590441,334.097153696005));
#37970=CARTESIAN_POINT('Ctrl Pts',(113.790364061427,-4.8579477161762,334.232193351554));
#37971=CARTESIAN_POINT('Ctrl Pts',(113.782600302031,-4.8793246208999,334.367446003626));
#37972=CARTESIAN_POINT('Ctrl Pts',(113.774836542635,-4.8950255443115,334.503444826225));
#37973=CARTESIAN_POINT('Ctrl Pts',(113.767072783239,-4.90503308943813,334.639675904196));
#37974=CARTESIAN_POINT('Ctrl Pts',(113.760227271669,-4.91385700610772,334.759794441221));
#37975=CARTESIAN_POINT('Ctrl Pts',(113.753381760099,-4.91825543465756,334.880093343675));
#37976=CARTESIAN_POINT('Ctrl Pts',(113.746536248529,-4.91824999495766,335.000222708279));
#37977=CARTESIAN_POINT('',(117.246536248536,-4.9182494855724,334.997750518554));
#37978=CARTESIAN_POINT('Ctrl Pts',(117.24653624849,-4.91824948557278,334.997750519371));
#37979=CARTESIAN_POINT('Ctrl Pts',(117.238656580834,-4.91831343288592,335.137564499501));
#37980=CARTESIAN_POINT('Ctrl Pts',(117.230776913178,-4.91241116676489,335.277359185831));
#37981=CARTESIAN_POINT('Ctrl Pts',(117.222897245522,-4.90057407742763,335.416601457204));
#37982=CARTESIAN_POINT('Ctrl Pts',(117.215014674906,-4.88873262717076,335.555895027028));
#37983=CARTESIAN_POINT('Ctrl Pts',(117.20713210429,-4.87095202893947,335.694635405755));
#37984=CARTESIAN_POINT('Ctrl Pts',(117.199249533674,-4.84731549143901,335.832295373624));
#37985=CARTESIAN_POINT('Ctrl Pts',(117.191362594417,-4.82366585420909,335.970031634745));
#37986=CARTESIAN_POINT('Ctrl Pts',(117.18347565516,-4.79415387465817,336.106685925741));
#37987=CARTESIAN_POINT('Ctrl Pts',(117.175588715903,-4.75891369292042,336.241742133389));
#37988=CARTESIAN_POINT('Ctrl Pts',(117.167690165343,-4.72362162991005,336.376997173382));
#37989=CARTESIAN_POINT('Ctrl Pts',(117.159791614782,-4.68258460953353,336.510649068882));
#37990=CARTESIAN_POINT('Ctrl Pts',(117.151893064222,-4.63598670297276,336.642196806829));
#37991=CARTESIAN_POINT('Ctrl Pts',(117.14398847896,-4.58935319438067,336.773845050722));
#37992=CARTESIAN_POINT('Ctrl Pts',(117.136083893698,-4.5371504680916,336.903385587463));
#37993=CARTESIAN_POINT('Ctrl Pts',(117.128179308437,-4.47961018621695,337.030338799817));
#37994=CARTESIAN_POINT('Ctrl Pts',(117.120260085878,-4.42196335426404,337.157527097476));
#37995=CARTESIAN_POINT('Ctrl Pts',(117.11234086332,-4.35895937967084,337.282118162656));
#37996=CARTESIAN_POINT('Ctrl Pts',(117.104421640762,-4.29087578559953,337.40365722495));
#37997=CARTESIAN_POINT('Ctrl Pts',(117.097403290715,-4.23053722432006,337.511370283553));
#37998=CARTESIAN_POINT('Ctrl Pts',(117.090384940669,-4.16620974209067,337.616686482591));
#37999=CARTESIAN_POINT('Ctrl Pts',(117.083366590622,-4.09811362679982,337.71931016332));
#38000=CARTESIAN_POINT('Ctrl Pts',(117.075591511844,-4.02267528910245,337.832998878889));
#38001=CARTESIAN_POINT('Ctrl Pts',(117.067816433065,-3.94238327911094,337.943725682216));
#38002=CARTESIAN_POINT('Ctrl Pts',(117.060041354287,-3.85749750858327,338.051048349957));
#38003=CARTESIAN_POINT('Ctrl Pts',(117.052275843238,-3.77271619540029,338.158238950323));
#38004=CARTESIAN_POINT('Ctrl Pts',(117.044510332189,-3.68335260952253,338.262033446382));
#38005=CARTESIAN_POINT('Ctrl Pts',(117.03674482114,-3.58971066051248,338.362017316479));
#38006=CARTESIAN_POINT('Ctrl Pts',(117.028987009617,-3.49616155776767,338.461902052277));
#38007=CARTESIAN_POINT('Ctrl Pts',(117.021229198095,-3.39834279920199,338.557983397584));
#38008=CARTESIAN_POINT('Ctrl Pts',(117.013471386573,-3.29659916595578,338.6498790393));
#38009=CARTESIAN_POINT('Ctrl Pts',(117.00571941305,-3.19493209802014,338.741705526631));
#38010=CARTESIAN_POINT('Ctrl Pts',(116.997967439527,-3.08934632328922,338.829352319102));
#38011=CARTESIAN_POINT('Ctrl Pts',(116.990215466004,-2.98022390189834,338.91247345768));
#38012=CARTESIAN_POINT('Ctrl Pts',(116.982466775446,-2.87114769391747,338.995559394408));
#38013=CARTESIAN_POINT('Ctrl Pts',(116.974718084889,-2.75853812853333,339.074123252902));
#38014=CARTESIAN_POINT('Ctrl Pts',(116.966969394331,-2.64281064164036,339.147859083302));
#38015=CARTESIAN_POINT('Ctrl Pts',(116.959222315953,-2.52710723281754,339.221579572347));
#38016=CARTESIAN_POINT('Ctrl Pts',(116.951475237575,-2.40828752225627,339.29047382144));
#38017=CARTESIAN_POINT('Ctrl Pts',(116.943728159198,-2.28679591309402,339.354279218695));
#38018=CARTESIAN_POINT('Ctrl Pts',(116.935981015892,-2.16530328571512,339.4180851507));
#38019=CARTESIAN_POINT('Ctrl Pts',(116.928233872586,-2.04113906112369,339.476801964059));
#38020=CARTESIAN_POINT('Ctrl Pts',(116.92048672928,-1.91477186555856,339.530213214118));
#38021=CARTESIAN_POINT('Ctrl Pts',(116.912737844252,-1.78837625996547,339.583636472159));
#38022=CARTESIAN_POINT('Ctrl Pts',(116.904988959224,-1.65977705782248,339.631751641209));
#38023=CARTESIAN_POINT('Ctrl Pts',(116.897240074196,-1.52946208463444,339.674390740424));
#38024=CARTESIAN_POINT('Ctrl Pts',(116.889482964421,-1.39900879378701,339.71707509722));
#38025=CARTESIAN_POINT('Ctrl Pts',(116.881725854646,-1.26683646608281,339.754271651707));
#38026=CARTESIAN_POINT('Ctrl Pts',(116.873968744872,-1.13344782004771,339.78586241985));
#38027=CARTESIAN_POINT('Ctrl Pts',(116.866207489946,-0.999987895385022,
339.817470069089));
#38028=CARTESIAN_POINT('Ctrl Pts',(116.858446235019,-0.865310740879716,
339.843465889031));
#38029=CARTESIAN_POINT('Ctrl Pts',(116.850684980093,-0.729927460062221,
339.863783400353));
#38030=CARTESIAN_POINT('Ctrl Pts',(116.842911309689,-0.59432761011691,339.884133413071));
#38031=CARTESIAN_POINT('Ctrl Pts',(116.835137639284,-0.458019765479544,
339.898786923957));
#38032=CARTESIAN_POINT('Ctrl Pts',(116.827363968879,-0.321519214412819,
339.90772946048));
#38033=CARTESIAN_POINT('Ctrl Pts',(116.819952164702,-0.191372796838107,
339.916255719777));
#38034=CARTESIAN_POINT('Ctrl Pts',(116.812540360525,-0.0610514977543804,
339.91959072367));
#38035=CARTESIAN_POINT('Ctrl Pts',(116.805128556348,0.0690014971030674,
339.917765941553));
#38036=CARTESIAN_POINT('Ctrl Pts',(116.79735347757,0.205428776646209,339.915851721428));
#38037=CARTESIAN_POINT('Ctrl Pts',(116.789578398791,0.341991921577325,339.908253084054));
#38038=CARTESIAN_POINT('Ctrl Pts',(116.781803320013,0.478178403686709,339.894949282347));
#38039=CARTESIAN_POINT('Ctrl Pts',(116.774037808964,0.614197299659894,339.881661851815));
#38040=CARTESIAN_POINT('Ctrl Pts',(116.766272297915,0.749840069754946,339.862683263506));
#38041=CARTESIAN_POINT('Ctrl Pts',(116.758506786866,0.884593670964688,339.838044760003));
#38042=CARTESIAN_POINT('Ctrl Pts',(116.750748975343,1.01921366358614,339.813430685647));
#38043=CARTESIAN_POINT('Ctrl Pts',(116.742991163821,1.15294585975989,339.78316793379));
#38044=CARTESIAN_POINT('Ctrl Pts',(116.735233352299,1.28528218338405,339.747339546691));
#38045=CARTESIAN_POINT('Ctrl Pts',(116.727481378776,1.41751891972823,339.711538121589));
#38046=CARTESIAN_POINT('Ctrl Pts',(116.719729405253,1.54836149859689,339.670179499622));
#38047=CARTESIAN_POINT('Ctrl Pts',(116.71197743173,1.6773122409977,339.623397745025));
#38048=CARTESIAN_POINT('Ctrl Pts',(116.704228741172,1.80620837268263,339.576635802528));
#38049=CARTESIAN_POINT('Ctrl Pts',(116.696480050615,1.93321389474144,339.524455428401));
#38050=CARTESIAN_POINT('Ctrl Pts',(116.688731360057,2.05784671120971,339.467040404526));
#38051=CARTESIAN_POINT('Ctrl Pts',(116.680984281679,2.18245359677939,339.409637326325));
#38052=CARTESIAN_POINT('Ctrl Pts',(116.673237203301,2.30468840389376,339.347001928142));
#38053=CARTESIAN_POINT('Ctrl Pts',(116.665490124924,2.42408980457841,339.279365803696));
#38054=CARTESIAN_POINT('Ctrl Pts',(116.657742981618,2.54349220596179,339.211729112393));
#38055=CARTESIAN_POINT('Ctrl Pts',(116.649995838312,2.66006081345148,339.139091803885));
#38056=CARTESIAN_POINT('Ctrl Pts',(116.642248695006,2.77336001357305,339.061730825352));
#38057=CARTESIAN_POINT('Ctrl Pts',(116.634499809978,2.88668468576037,338.984352454428));
#38058=CARTESIAN_POINT('Ctrl Pts',(116.62675092495,2.99673816520765,338.902248520623));
#38059=CARTESIAN_POINT('Ctrl Pts',(116.619002039922,3.10311520286695,338.815738342737));
#38060=CARTESIAN_POINT('Ctrl Pts',(116.611244930147,3.20960515021311,338.729136342055));
#38061=CARTESIAN_POINT('Ctrl Pts',(116.603487820372,3.31241055700217,338.638119001886));
#38062=CARTESIAN_POINT('Ctrl Pts',(116.595730710598,3.4111601581012,338.543045221033));
#38063=CARTESIAN_POINT('Ctrl Pts',(116.587969455671,3.50996252782953,338.447920635791));
#38064=CARTESIAN_POINT('Ctrl Pts',(116.580208200745,3.6047045034919,338.348735573167));
#38065=CARTESIAN_POINT('Ctrl Pts',(116.572446945819,3.69505359375842,338.245883855247));
#38066=CARTESIAN_POINT('Ctrl Pts',(116.564673275414,3.78554721312473,338.142867608097));
#38067=CARTESIAN_POINT('Ctrl Pts',(116.55689960501,3.87163365912346,338.0361732891));
#38068=CARTESIAN_POINT('Ctrl Pts',(116.549125934605,3.95302190944854,337.926226383231));
#38069=CARTESIAN_POINT('Ctrl Pts',(116.541714130428,4.0306215171394,337.821397532284));
#38070=CARTESIAN_POINT('Ctrl Pts',(116.534302326251,4.10395032583083,337.713612333572));
#38071=CARTESIAN_POINT('Ctrl Pts',(116.526890522074,4.17279496557417,337.603260501329));
#38072=CARTESIAN_POINT('Ctrl Pts',(116.519115443296,4.24501388618956,337.487499997065));
#38073=CARTESIAN_POINT('Ctrl Pts',(116.511340364517,4.31252618362558,337.368549076353));
#38074=CARTESIAN_POINT('Ctrl Pts',(116.503565285739,4.37503705279395,337.246827507661));
#38075=CARTESIAN_POINT('Ctrl Pts',(116.49579977469,4.43747099835817,337.125255725107));
#38076=CARTESIAN_POINT('Ctrl Pts',(116.488034263641,4.4949155846381,337.000920422798));
#38077=CARTESIAN_POINT('Ctrl Pts',(116.480268752592,4.54711944717708,336.874269936696));
#38078=CARTESIAN_POINT('Ctrl Pts',(116.47251094107,4.5992715494343,336.74774502492));
#38079=CARTESIAN_POINT('Ctrl Pts',(116.464753129547,4.64619312067145,336.6189098566));
#38080=CARTESIAN_POINT('Ctrl Pts',(116.456995318025,4.68767904376461,336.488236622702));
#38081=CARTESIAN_POINT('Ctrl Pts',(116.449243344502,4.72913374738513,336.357661724555));
#38082=CARTESIAN_POINT('Ctrl Pts',(116.441491370979,4.76516082699687,336.225251885076));
#38083=CARTESIAN_POINT('Ctrl Pts',(116.433739397456,4.79560369741601,336.091498162999));
#38084=CARTESIAN_POINT('Ctrl Pts',(116.425990706898,4.8260336752614,335.957801085702));
#38085=CARTESIAN_POINT('Ctrl Pts',(116.418242016341,4.85088406099985,335.82276163811));
#38086=CARTESIAN_POINT('Ctrl Pts',(116.410493325783,4.87004851094776,335.686884679925));
#38087=CARTESIAN_POINT('Ctrl Pts',(116.402746247405,4.88920897357179,335.551035992076));
#38088=CARTESIAN_POINT('Ctrl Pts',(116.394999169028,4.90268579893338,335.414350527033));
#38089=CARTESIAN_POINT('Ctrl Pts',(116.38725209065,4.91042408809411,335.277341553982));
#38090=CARTESIAN_POINT('Ctrl Pts',(116.379504947344,4.91816244210915,335.140331432664));
#38091=CARTESIAN_POINT('Ctrl Pts',(116.371757804038,4.9201621419538,335.002998188182));
#38092=CARTESIAN_POINT('Ctrl Pts',(116.364010660732,4.91642034297385,334.865858009211));
#38093=CARTESIAN_POINT('Ctrl Pts',(116.356261775704,4.91267770275806,334.728686998216));
#38094=CARTESIAN_POINT('Ctrl Pts',(116.348512890676,4.9031910058071,334.591709529757));
#38095=CARTESIAN_POINT('Ctrl Pts',(116.340764005648,4.88800947059981,334.455439188128));
#38096=CARTESIAN_POINT('Ctrl Pts',(116.333006895873,4.87281182155416,334.31902420775));
#38097=CARTESIAN_POINT('Ctrl Pts',(116.325249786099,4.85190730302309,334.183318242585));
#38098=CARTESIAN_POINT('Ctrl Pts',(116.317492676324,4.82539680779922,334.048827718139));
#38099=CARTESIAN_POINT('Ctrl Pts',(116.309731421398,4.79887214621431,333.914265326256));
#38100=CARTESIAN_POINT('Ctrl Pts',(116.301970166472,4.76673563035788,333.780920049067));
#38101=CARTESIAN_POINT('Ctrl Pts',(116.294208911545,4.72913850348643,333.649284605351));
#38102=CARTESIAN_POINT('Ctrl Pts',(116.286435241141,4.69148123346491,333.517438587825));
#38103=CARTESIAN_POINT('Ctrl Pts',(116.278661570736,4.64834601996584,333.387308240683));
#38104=CARTESIAN_POINT('Ctrl Pts',(116.270887900331,4.59993317351458,333.259368545125));
#38105=CARTESIAN_POINT('Ctrl Pts',(116.263476096154,4.55377395671318,333.137384473176));
#38106=CARTESIAN_POINT('Ctrl Pts',(116.256064291977,4.50281750960875,333.017391957809));
#38107=CARTESIAN_POINT('Ctrl Pts',(116.2486524878,4.44727608449179,332.899781323098));
#38108=CARTESIAN_POINT('Ctrl Pts',(116.240877409022,4.38901240868031,332.776406240836));
#38109=CARTESIAN_POINT('Ctrl Pts',(116.233102330243,4.32551881974418,332.655262541011));
#38110=CARTESIAN_POINT('Ctrl Pts',(116.225327251465,4.25698877399473,332.536825292314));
#38111=CARTESIAN_POINT('Ctrl Pts',(116.217561740416,4.1885430588296,332.418533788193));
#38112=CARTESIAN_POINT('Ctrl Pts',(116.209796229367,4.11507341234639,332.302942443626));
#38113=CARTESIAN_POINT('Ctrl Pts',(116.202030718318,4.03682082209073,332.190505256664));
#38114=CARTESIAN_POINT('Ctrl Pts',(116.194272906796,3.95864581950602,332.078179551499));
#38115=CARTESIAN_POINT('Ctrl Pts',(116.186515095274,3.87569753244349,331.96900209908));
#38116=CARTESIAN_POINT('Ctrl Pts',(116.178757283752,3.78826203571425,331.863400916396));
#38117=CARTESIAN_POINT('Ctrl Pts',(116.171005310229,3.70089233696875,331.757879201951));
#38118=CARTESIAN_POINT('Ctrl Pts',(116.163253336706,3.60904239812246,331.655928700284));
#38119=CARTESIAN_POINT('Ctrl Pts',(116.155501363183,3.51304042371204,331.557946827275));
#38120=CARTESIAN_POINT('Ctrl Pts',(116.147752672625,3.41707910619497,331.460006449648));
#38121=CARTESIAN_POINT('Ctrl Pts',(116.140003982067,3.316969523412,331.366031636466));
#38122=CARTESIAN_POINT('Ctrl Pts',(116.13225529151,3.21307867398919,331.276385022957));
#38123=CARTESIAN_POINT('Ctrl Pts',(116.124508213132,3.10920943992531,331.186757061175));
#38124=CARTESIAN_POINT('Ctrl Pts',(116.116761134754,3.00156079981723,331.101455763068));
#38125=CARTESIAN_POINT('Ctrl Pts',(116.109014056376,2.89053466370803,331.020805053732));
#38126=CARTESIAN_POINT('Ctrl Pts',(116.10126691307,2.77950759709302,330.940153668466));
#38127=CARTESIAN_POINT('Ctrl Pts',(116.093519769765,2.6651032942607,330.864153179436));
#38128=CARTESIAN_POINT('Ctrl Pts',(116.085772626459,2.54775428987424,330.793085318083));
#38129=CARTESIAN_POINT('Ctrl Pts',(116.078023741431,2.4303789029403,330.722001479166));
#38130=CARTESIAN_POINT('Ctrl Pts',(116.070274856403,2.31005783135975,330.655852677073));
#38131=CARTESIAN_POINT('Ctrl Pts',(116.062525971375,2.18724959406665,330.594875452867));
#38132=CARTESIAN_POINT('Ctrl Pts',(116.0547688616,2.06431100684147,330.533833506805));
#38133=CARTESIAN_POINT('Ctrl Pts',(116.047011751825,1.93888033109602,330.477974277858));
#38134=CARTESIAN_POINT('Ctrl Pts',(116.03925464205,1.81143802972191,330.427486979026));
#38135=CARTESIAN_POINT('Ctrl Pts',(116.031493387124,1.68392762725658,330.376972701395));
#38136=CARTESIAN_POINT('Ctrl Pts',(116.023732132198,1.55440382614832,330.331836202344));
#38137=CARTESIAN_POINT('Ctrl Pts',(116.015970877272,1.42336281053587,330.292216936595));
#38138=CARTESIAN_POINT('Ctrl Pts',(116.008197206867,1.29211217200488,330.252534292933));
#38139=CARTESIAN_POINT('Ctrl Pts',(116.000423536463,1.15933984776138,330.218386616497));
#38140=CARTESIAN_POINT('Ctrl Pts',(115.992649866058,1.02555365914964,330.189862501476));
#38141=CARTESIAN_POINT('Ctrl Pts',(115.985238061881,0.897995249804329,330.162666190872));
#38142=CARTESIAN_POINT('Ctrl Pts',(115.977826257704,0.769515526294496,330.140581719116));
#38143=CARTESIAN_POINT('Ctrl Pts',(115.970414453527,0.640557582355683,330.123641825482));
#38144=CARTESIAN_POINT('Ctrl Pts',(115.962639374748,0.505279025439115,330.105871657201));
#38145=CARTESIAN_POINT('Ctrl Pts',(115.95486429597,0.36904667953373,330.093706963514));
#38146=CARTESIAN_POINT('Ctrl Pts',(115.947089217191,0.232364730348951,330.087242149811));
#38147=CARTESIAN_POINT('Ctrl Pts',(115.939323706142,0.0958509770039653,
330.080785291474));
#38148=CARTESIAN_POINT('Ctrl Pts',(115.931558195093,-0.0411108920754093,
330.080014375433));
#38149=CARTESIAN_POINT('Ctrl Pts',(115.923792684044,-0.178008688054912,
330.084972434515));
#38150=CARTESIAN_POINT('Ctrl Pts',(115.916034872522,-0.314770749470483,
330.089925577667));
#38151=CARTESIAN_POINT('Ctrl Pts',(115.908277061,-0.451468476109896,330.100596377777));
#38152=CARTESIAN_POINT('Ctrl Pts',(115.900519249478,-0.587587127858695,
330.116975892987));
#38153=CARTESIAN_POINT('Ctrl Pts',(115.892767275955,-0.723603346005389,
330.133343082091));
#38154=CARTESIAN_POINT('Ctrl Pts',(115.885015302432,-0.859040970132618,
330.155410388829));
#38155=CARTESIAN_POINT('Ctrl Pts',(115.877263328909,-0.993388194442216,
330.183116883539));
#38156=CARTESIAN_POINT('Ctrl Pts',(115.869514638351,-1.12767852262311,330.210811644533));
#38157=CARTESIAN_POINT('Ctrl Pts',(115.861765947794,-1.26087898742259,330.244140764753));
#38158=CARTESIAN_POINT('Ctrl Pts',(115.854017257236,-1.39248603712727,330.282991869956));
#38159=CARTESIAN_POINT('Ctrl Pts',(115.846270178858,-1.52406570488586,330.321834891861));
#38160=CARTESIAN_POINT('Ctrl Pts',(115.83852310048,-1.65405224232759,330.366197502918));
#38161=CARTESIAN_POINT('Ctrl Pts',(115.830776022102,-1.78195575734221,330.415917022852));
#38162=CARTESIAN_POINT('Ctrl Pts',(115.823028878797,-1.9098603443114,330.465636959484));
#38163=CARTESIAN_POINT('Ctrl Pts',(115.815281735491,-2.03568150971615,330.520713752924));
#38164=CARTESIAN_POINT('Ctrl Pts',(115.807534592185,-2.15894827025205,330.580936136592));
#38165=CARTESIAN_POINT('Ctrl Pts',(115.799785707157,-2.28224274377249,330.641172059531));
#38166=CARTESIAN_POINT('Ctrl Pts',(115.792036822129,-2.40298131852899,330.706555703131));
#38167=CARTESIAN_POINT('Ctrl Pts',(115.784287937101,-2.52071695119039,330.776829494979));
#38168=CARTESIAN_POINT('Ctrl Pts',(115.776530827326,-2.63857754966897,330.847177876156));
#38169=CARTESIAN_POINT('Ctrl Pts',(115.768773717551,-2.75342850285078,330.922426573351));
#38170=CARTESIAN_POINT('Ctrl Pts',(115.761016607776,-2.86485069144925,331.00227394908));
#38171=CARTESIAN_POINT('Ctrl Pts',(115.75325535285,-2.97633242050287,331.082163992694));
#38172=CARTESIAN_POINT('Ctrl Pts',(115.745494097924,-3.08438142635394,331.166657370746));
#38173=CARTESIAN_POINT('Ctrl Pts',(115.737732842998,-3.18861192484192,331.255412298362));
#38174=CARTESIAN_POINT('Ctrl Pts',(115.729959172593,-3.2930091581587,331.344309204937));
#38175=CARTESIAN_POINT('Ctrl Pts',(115.722185502189,-3.39357539090462,331.437481017854));
#38176=CARTESIAN_POINT('Ctrl Pts',(115.714411831784,-3.48996131106872,331.53454864271));
#38177=CARTESIAN_POINT('Ctrl Pts',(115.707000027607,-3.58186044346053,331.627097746276));
#38178=CARTESIAN_POINT('Ctrl Pts',(115.69958822343,-3.66995949746807,331.723187911896));
#38179=CARTESIAN_POINT('Ctrl Pts',(115.692176419253,-3.75399115849184,331.822464249695));
#38180=CARTESIAN_POINT('Ctrl Pts',(115.684448837586,-3.84160296090546,331.925970223344));
#38181=CARTESIAN_POINT('Ctrl Pts',(115.67672125592,-3.92508001115426,332.03327892309));
#38182=CARTESIAN_POINT('Ctrl Pts',(115.668993674254,-4.0040708182706,332.144023819292));
#38183=CARTESIAN_POINT('Ctrl Pts',(115.66127857742,-4.08293400629399,332.254589793873));
#38184=CARTESIAN_POINT('Ctrl Pts',(115.653563480586,-4.15732515638901,332.368580590616));
#38185=CARTESIAN_POINT('Ctrl Pts',(115.645848383752,-4.22693171934945,332.485595238937));
#38186=CARTESIAN_POINT('Ctrl Pts',(115.638140515054,-4.29647306917115,332.602500258335));
#38187=CARTESIAN_POINT('Ctrl Pts',(115.630432646356,-4.36123854570563,332.722423157182));
#38188=CARTESIAN_POINT('Ctrl Pts',(115.622724777658,-4.42095763075255,332.844932323663));
#38189=CARTESIAN_POINT('Ctrl Pts',(115.615022409018,-4.48063410240012,332.967354071993));
#38190=CARTESIAN_POINT('Ctrl Pts',(115.607320040379,-4.53527117295905,333.092358062275));
#38191=CARTESIAN_POINT('Ctrl Pts',(115.599617671739,-4.58464343942483,333.219486704391));
#38192=CARTESIAN_POINT('Ctrl Pts',(115.591919079466,-4.63399149934459,333.346553017076));
#38193=CARTESIAN_POINT('Ctrl Pts',(115.584220487192,-4.67807974880975,333.475741540178));
#38194=CARTESIAN_POINT('Ctrl Pts',(115.576521894919,-4.71673045205952,333.606573681491));
#38195=CARTESIAN_POINT('Ctrl Pts',(115.568824079112,-4.75537725706688,333.737392627302));
#38196=CARTESIAN_POINT('Ctrl Pts',(115.561126263305,-4.78858748724757,333.869854484083));
#38197=CARTESIAN_POINT('Ctrl Pts',(115.553428447498,-4.81623300248729,334.003464637731));
#38198=CARTESIAN_POINT('Ctrl Pts',(115.545731117604,-4.84387677264664,334.137066357445));
#38199=CARTESIAN_POINT('Ctrl Pts',(115.53803378771,-4.86595645195465,334.271815840756));
#38200=CARTESIAN_POINT('Ctrl Pts',(115.530336457815,-4.88239499323559,334.407208137262));
#38201=CARTESIAN_POINT('Ctrl Pts',(115.522635710278,-4.89884083328964,334.542660548449));
#38202=CARTESIAN_POINT('Ctrl Pts',(115.514934962741,-4.90964049051541,334.678755948844));
#38203=CARTESIAN_POINT('Ctrl Pts',(115.507234215204,-4.91476878400503,334.814984156706));
#38204=CARTESIAN_POINT('Ctrl Pts',(115.503668226299,-4.91714354536363,334.878067419128));
#38205=CARTESIAN_POINT('Ctrl Pts',(115.500102237395,-4.91830290451448,334.941179132723));
#38206=CARTESIAN_POINT('Ctrl Pts',(115.49653624849,-4.91824814755945,335.004268668182));
#38207=CARTESIAN_POINT('',(118.996536248454,-4.91824887548736,334.996674151641));
#38208=CARTESIAN_POINT('Ctrl Pts',(118.996536248454,-4.91824887548736,334.996674151641));
#38209=CARTESIAN_POINT('Ctrl Pts',(118.988875843359,-4.91833997688369,335.131394467091));
#38210=CARTESIAN_POINT('Ctrl Pts',(118.981215438265,-4.9128915405517,335.266331852603));
#38211=CARTESIAN_POINT('Ctrl Pts',(118.97355503317,-4.9018765637506,335.400985306779));
#38212=CARTESIAN_POINT('Ctrl Pts',(118.965902782214,-4.89087331186996,335.535495428738));
#38213=CARTESIAN_POINT('Ctrl Pts',(118.958250531257,-4.87431533657838,335.669721822289));
#38214=CARTESIAN_POINT('Ctrl Pts',(118.950598280301,-4.85222765334842,335.803162413576));
#38215=CARTESIAN_POINT('Ctrl Pts',(118.942952224206,-4.83015785115041,335.936494978346));
#38216=CARTESIAN_POINT('Ctrl Pts',(118.935306168111,-4.80256731158553,336.069042610921));
#38217=CARTESIAN_POINT('Ctrl Pts',(118.927660112016,-4.76953291471938,336.200307809651));
#38218=CARTESIAN_POINT('Ctrl Pts',(118.92001772895,-4.73651438698541,336.331509950932));
#38219=CARTESIAN_POINT('Ctrl Pts',(118.912375345883,-4.69805729946584,336.461430493612));
#38220=CARTESIAN_POINT('Ctrl Pts',(118.904732962817,-4.65428965003596,336.589581994132));
#38221=CARTESIAN_POINT('Ctrl Pts',(118.897092344035,-4.61053210459963,336.7177039102));
#38222=CARTESIAN_POINT('Ctrl Pts',(118.889451725253,-4.5614665646002,336.844057215134));
#38223=CARTESIAN_POINT('Ctrl Pts',(118.881811106471,-4.50727077723995,336.968170013779));
#38224=CARTESIAN_POINT('Ctrl Pts',(118.874170489986,-4.45307500616858,337.092282775121));
#38225=CARTESIAN_POINT('Ctrl Pts',(118.8665298735,-4.39374915218029,337.214154662487));
#38226=CARTESIAN_POINT('Ctrl Pts',(118.858889257015,-4.32951872896555,337.333334660531));
#38227=CARTESIAN_POINT('Ctrl Pts',(118.851246881055,-4.26527351482691,337.452542103237));
#38228=CARTESIAN_POINT('Ctrl Pts',(118.843604505096,-4.19612167703267,337.569056069762));
#38229=CARTESIAN_POINT('Ctrl Pts',(118.835962129136,-4.12233392781025,337.682451500051));
#38230=CARTESIAN_POINT('Ctrl Pts',(118.828311845355,-4.04846982794068,337.795964264376));
#38231=CARTESIAN_POINT('Ctrl Pts',(118.820661561574,-3.9699604592865,337.906351712053));
#38232=CARTESIAN_POINT('Ctrl Pts',(118.813011277792,-3.88711916257599,338.013218823523));
#38233=CARTESIAN_POINT('Ctrl Pts',(118.805356671563,-3.80423106012154,338.120146315441));
#38234=CARTESIAN_POINT('Ctrl Pts',(118.797702065333,-3.71700641623412,338.22354920428));
#38235=CARTESIAN_POINT('Ctrl Pts',(118.790047459104,-3.62579696872232,338.323067770014));
#38236=CARTESIAN_POINT('Ctrl Pts',(118.782381461024,-3.53445178014621,338.42273444273));
#38237=CARTESIAN_POINT('Ctrl Pts',(118.774715462944,-3.43911023079049,338.518504965712));
#38238=CARTESIAN_POINT('Ctrl Pts',(118.767049464864,-3.3401591307308,338.610058177356));
#38239=CARTESIAN_POINT('Ctrl Pts',(118.762297908664,-3.27882703698147,338.666804895242));
#38240=CARTESIAN_POINT('Ctrl Pts',(118.757546352465,-3.21610887156023,338.721932217824));
#38241=CARTESIAN_POINT('Ctrl Pts',(118.752794796265,-3.15210235561836,338.775372008452));
#38242=CARTESIAN_POINT('Ctrl Pts',(118.745019717487,-3.04736704724914,338.862816745418));
#38243=CARTESIAN_POINT('Ctrl Pts',(118.737244638709,-2.93882467881816,338.946038053379));
#38244=CARTESIAN_POINT('Ctrl Pts',(118.72946955993,-2.82685051373547,339.024686228204));
#38245=CARTESIAN_POINT('Ctrl Pts',(118.721704048881,-2.71501413999145,339.103237621442));
#38246=CARTESIAN_POINT('Ctrl Pts',(118.713938537832,-2.59975468904415,339.177226856203));
#38247=CARTESIAN_POINT('Ctrl Pts',(118.706173026783,-2.48148169156554,339.246343330081));
#38248=CARTESIAN_POINT('Ctrl Pts',(118.698415215261,-2.3633259621084,339.315391274774));
#38249=CARTESIAN_POINT('Ctrl Pts',(118.690657403739,-2.24216296759089,339.379575877312));
#38250=CARTESIAN_POINT('Ctrl Pts',(118.682899592217,-2.11843222396238,339.43862906481));
#38251=CARTESIAN_POINT('Ctrl Pts',(118.675147618694,-1.99479459164251,339.497637812912));
#38252=CARTESIAN_POINT('Ctrl Pts',(118.667395645171,-1.86859340772187,339.551522664521));
#38253=CARTESIAN_POINT('Ctrl Pts',(118.659643671648,-1.74029354754665,339.60006102469));
#38254=CARTESIAN_POINT('Ctrl Pts',(118.65189498109,-1.61204802243807,339.648578828834));
#38255=CARTESIAN_POINT('Ctrl Pts',(118.644146290532,-1.48170595364246,339.691754506935));
#38256=CARTESIAN_POINT('Ctrl Pts',(118.636397599975,-1.3497527921755,339.729413331748));
#38257=CARTESIAN_POINT('Ctrl Pts',(118.628650521597,-1.21782708466583,339.767064321327));
#38258=CARTESIAN_POINT('Ctrl Pts',(118.620903443219,-1.08429132685455,339.799200633525));
#38259=CARTESIAN_POINT('Ctrl Pts',(118.613156364841,-0.949646370496838,
339.82569734168));
#38260=CARTESIAN_POINT('Ctrl Pts',(118.605409221535,-0.815000285684848,
339.852194271904));
#38261=CARTESIAN_POINT('Ctrl Pts',(118.59766207823,-0.679245367303301,339.87305142834));
#38262=CARTESIAN_POINT('Ctrl Pts',(118.589914934924,-0.542892513740601,
339.888195043267));
#38263=CARTESIAN_POINT('Ctrl Pts',(118.582166049896,-0.406509005161195,
339.903342062801));
#38264=CARTESIAN_POINT('Ctrl Pts',(118.574417164868,-0.269527682312667,
339.912772941627));
#38265=CARTESIAN_POINT('Ctrl Pts',(118.56666827984,-0.132464019994088,339.916465838985));
#38266=CARTESIAN_POINT('Ctrl Pts',(118.558911170065,0.00474512311143449,
339.920162656022));
#38267=CARTESIAN_POINT('Ctrl Pts',(118.55115406029,0.142036388918992,339.918109314995));
#38268=CARTESIAN_POINT('Ctrl Pts',(118.543396950515,0.278894290845277,339.910336142978));
#38269=CARTESIAN_POINT('Ctrl Pts',(118.535635695589,0.415825325258531,339.902558817225));
#38270=CARTESIAN_POINT('Ctrl Pts',(118.527874440663,0.552322145576616,339.889055608601));
#38271=CARTESIAN_POINT('Ctrl Pts',(118.520113185737,0.68787592118284,339.86990860074));
#38272=CARTESIAN_POINT('Ctrl Pts',(118.512339515332,0.823646538653116,339.850730963905));
#38273=CARTESIAN_POINT('Ctrl Pts',(118.504565844928,0.958470712246472,339.825891557595));
#38274=CARTESIAN_POINT('Ctrl Pts',(118.496792174523,1.09185043628403,339.795523505029));
#38275=CARTESIAN_POINT('Ctrl Pts',(118.489380370346,1.21902130207793,339.766569092616));
#38276=CARTESIAN_POINT('Ctrl Pts',(118.481968566169,1.34487889237259,339.732589242545));
#38277=CARTESIAN_POINT('Ctrl Pts',(118.474556761992,1.46900741371671,339.693740542568));
#38278=CARTESIAN_POINT('Ctrl Pts',(118.466781683213,1.59921984365208,339.652987752081));
#38279=CARTESIAN_POINT('Ctrl Pts',(118.459006604435,1.7279409206832,339.606747983793));
#38280=CARTESIAN_POINT('Ctrl Pts',(118.451231525657,1.85467349458063,339.555147559739));
#38281=CARTESIAN_POINT('Ctrl Pts',(118.443466014608,1.9812501159779,339.503610633293));
#38282=CARTESIAN_POINT('Ctrl Pts',(118.435700503559,2.1058427444732,339.44672632247));
#38283=CARTESIAN_POINT('Ctrl Pts',(118.42793499251,2.22796856733121,339.384670925564));
#38284=CARTESIAN_POINT('Ctrl Pts',(118.420177180987,2.34997330207991,339.322677056765));
#38285=CARTESIAN_POINT('Ctrl Pts',(118.412419369465,2.46951575233738,339.255522481121));
#38286=CARTESIAN_POINT('Ctrl Pts',(118.404661557943,2.58613264259454,339.183431727351));
#38287=CARTESIAN_POINT('Ctrl Pts',(118.39690958442,2.70266177494385,339.111395224159));
#38288=CARTESIAN_POINT('Ctrl Pts',(118.389157610897,2.81626939828716,339.034430141333));
#38289=CARTESIAN_POINT('Ctrl Pts',(118.381405637374,2.92651675705899,338.952806943572));
#38290=CARTESIAN_POINT('Ctrl Pts',(118.373656946816,3.03671742600892,338.871218313284));
#38291=CARTESIAN_POINT('Ctrl Pts',(118.365908256259,3.14356034728874,338.784975723748));
#38292=CARTESIAN_POINT('Ctrl Pts',(118.358159565701,3.24663588362999,338.694392846142));
#38293=CARTESIAN_POINT('Ctrl Pts',(118.350412487323,3.349689974245,338.603828815061));
#38294=CARTESIAN_POINT('Ctrl Pts',(118.342665408945,3.44897794560169,338.508926549968));
#38295=CARTESIAN_POINT('Ctrl Pts',(118.334918330568,3.5441237045835,338.410039622806));
#38296=CARTESIAN_POINT('Ctrl Pts',(118.327171187262,3.6392702609785,338.311151866877));
#38297=CARTESIAN_POINT('Ctrl Pts',(118.319424043956,3.7302742647451,338.208279663936));
#38298=CARTESIAN_POINT('Ctrl Pts',(118.31167690065,3.81679720660061,338.101812719393));
#38299=CARTESIAN_POINT('Ctrl Pts',(118.303928015622,3.90333960065008,337.99532183882));
#38300=CARTESIAN_POINT('Ctrl Pts',(118.296179130594,3.98539868163359,337.885234911745));
#38301=CARTESIAN_POINT('Ctrl Pts',(118.288430245566,4.06267713019773,337.771973592635));
#38302=CARTESIAN_POINT('Ctrl Pts',(118.280673135791,4.14003760290573,337.658592056791));
#38303=CARTESIAN_POINT('Ctrl Pts',(118.272916026017,4.21260708633004,337.542029721743));
#38304=CARTESIAN_POINT('Ctrl Pts',(118.265158916242,4.28013212378407,337.422736482875));
#38305=CARTESIAN_POINT('Ctrl Pts',(118.257397661316,4.34769324445904,337.303379497514));
#38306=CARTESIAN_POINT('Ctrl Pts',(118.249636406389,4.41020436990875,337.181289048276));
#38307=CARTESIAN_POINT('Ctrl Pts',(118.241875151463,4.46745916856873,337.056937441847));
#38308=CARTESIAN_POINT('Ctrl Pts',(118.234101481059,4.52480555624725,336.932386913373));
#38309=CARTESIAN_POINT('Ctrl Pts',(118.226327810654,4.57687866609643,336.805568361412));
#38310=CARTESIAN_POINT('Ctrl Pts',(118.218554140249,4.62352094482344,336.676972610176));
#38311=CARTESIAN_POINT('Ctrl Pts',(118.211142336072,4.66799201425439,336.554363022097));
#38312=CARTESIAN_POINT('Ctrl Pts',(118.203730531895,4.70752639721672,336.430138242727));
#38313=CARTESIAN_POINT('Ctrl Pts',(118.196318727718,4.74203076199793,336.304732660266));
#38314=CARTESIAN_POINT('Ctrl Pts',(118.18854364894,4.7782262884802,336.173180576646));
#38315=CARTESIAN_POINT('Ctrl Pts',(118.180768570161,4.80900064164011,336.039913284969));
#38316=CARTESIAN_POINT('Ctrl Pts',(118.172993491383,4.83419101185646,335.90541720957));
#38317=CARTESIAN_POINT('Ctrl Pts',(118.165227980334,4.85935038371852,335.771086640156));
#38318=CARTESIAN_POINT('Ctrl Pts',(118.157462469285,4.87893937357584,335.63553067618));
#38319=CARTESIAN_POINT('Ctrl Pts',(118.149696958236,4.89284495675063,335.499250730295));
#38320=CARTESIAN_POINT('Ctrl Pts',(118.141939146713,4.90673675249929,335.363105906373));
#38321=CARTESIAN_POINT('Ctrl Pts',(118.134181335191,4.9149563163394,335.226238915415));
#38322=CARTESIAN_POINT('Ctrl Pts',(118.126423523669,4.91744175429895,335.089160841053));
#38323=CARTESIAN_POINT('Ctrl Pts',(118.118671550146,4.91992532188761,334.95218592229));
#38324=CARTESIAN_POINT('Ctrl Pts',(118.110919576623,4.91668334555691,334.815000625536));
#38325=CARTESIAN_POINT('Ctrl Pts',(118.1031676031,4.90770582902847,334.678120273674));
#38326=CARTESIAN_POINT('Ctrl Pts',(118.095418912542,4.89873211448361,334.541297890722));
#38327=CARTESIAN_POINT('Ctrl Pts',(118.087670221985,4.88402771638807,334.404780585027));
#38328=CARTESIAN_POINT('Ctrl Pts',(118.079921531427,4.86363472929568,334.269082574781));
#38329=CARTESIAN_POINT('Ctrl Pts',(118.072174453049,4.84324598513459,334.133412797639));
#38330=CARTESIAN_POINT('Ctrl Pts',(118.064427374672,4.81717106421079,333.998562363177));
#38331=CARTESIAN_POINT('Ctrl Pts',(118.056680296294,4.78550376714829,333.865038874186));
#38332=CARTESIAN_POINT('Ctrl Pts',(118.048933152988,4.75383620468341,333.73151426614));
#38333=CARTESIAN_POINT('Ctrl Pts',(118.041186009682,4.71657626279533,333.59931700607));
#38334=CARTESIAN_POINT('Ctrl Pts',(118.033438866376,4.6738684662794,333.468942645614));
#38335=CARTESIAN_POINT('Ctrl Pts',(118.025689981348,4.63115106814392,333.338538974233));
#38336=CARTESIAN_POINT('Ctrl Pts',(118.01794109632,4.58298349983442,333.209959389353));
#38337=CARTESIAN_POINT('Ctrl Pts',(118.010192211292,4.52955944302532,333.083682094589));
#38338=CARTESIAN_POINT('Ctrl Pts',(118.002435101517,4.47607868137037,332.957270767799));
#38339=CARTESIAN_POINT('Ctrl Pts',(117.994677991743,4.41733043859673,332.833166973145));
#38340=CARTESIAN_POINT('Ctrl Pts',(117.986920881968,4.35355588137484,332.71182731197));
#38341=CARTESIAN_POINT('Ctrl Pts',(117.979159627042,4.28974724506864,332.59042281076));
#38342=CARTESIAN_POINT('Ctrl Pts',(117.971398372115,4.22090713848748,332.471785724121));
#38343=CARTESIAN_POINT('Ctrl Pts',(117.963637117189,4.14732107655037,332.356345152918));
#38344=CARTESIAN_POINT('Ctrl Pts',(117.955863446785,4.07361730089588,332.240719914422));
#38345=CARTESIAN_POINT('Ctrl Pts',(117.94808977638,3.99515262269015,332.128301730106));
#38346=CARTESIAN_POINT('Ctrl Pts',(117.940316105975,3.91225452535773,332.019488703038));
#38347=CARTESIAN_POINT('Ctrl Pts',(117.932904301798,3.8332153544005,331.915740948559));
#38348=CARTESIAN_POINT('Ctrl Pts',(117.925492497621,3.7501464103122,331.815270486364));
#38349=CARTESIAN_POINT('Ctrl Pts',(117.918080693444,3.66336247225411,331.718390873462));
#38350=CARTESIAN_POINT('Ctrl Pts',(117.910305614666,3.57232499487551,331.616762902141));
#38351=CARTESIAN_POINT('Ctrl Pts',(117.902530535887,3.47691145449798,331.518765513625));
#38352=CARTESIAN_POINT('Ctrl Pts',(117.894755457109,3.37744279009486,331.424798850115));
#38353=CARTESIAN_POINT('Ctrl Pts',(117.88698994606,3.27809652821564,331.330947818568));
#38354=CARTESIAN_POINT('Ctrl Pts',(117.879224435011,3.17470535257591,331.241117908777));
#38355=CARTESIAN_POINT('Ctrl Pts',(117.871458923962,3.06762974763401,331.155675508762));
#38356=CARTESIAN_POINT('Ctrl Pts',(117.863701112439,2.96066030846611,331.070317825136));
#38357=CARTESIAN_POINT('Ctrl Pts',(117.855943300917,2.85001401347286,330.989339236313));
#38358=CARTESIAN_POINT('Ctrl Pts',(117.848185489395,2.73608714940386,330.913068366933));
#38359=CARTESIAN_POINT('Ctrl Pts',(117.840433515872,2.6222460189125,330.8368548938));
#38360=CARTESIAN_POINT('Ctrl Pts',(117.832681542349,2.50512955673429,330.765342305097));
#38361=CARTESIAN_POINT('Ctrl Pts',(117.824929568826,2.38516569931506,330.698817877686));
#38362=CARTESIAN_POINT('Ctrl Pts',(117.817180878268,2.26525264666126,330.632321623411));
#38363=CARTESIAN_POINT('Ctrl Pts',(117.809432187711,2.14249493828591,330.570809518001));
#38364=CARTESIAN_POINT('Ctrl Pts',(117.801683497153,2.01734777101439,330.514524436218));
#38365=CARTESIAN_POINT('Ctrl Pts',(117.793936418775,1.89222664165648,330.458251065017));
#38366=CARTESIAN_POINT('Ctrl Pts',(117.786189340397,1.76471739851877,330.407202714502));
#38367=CARTESIAN_POINT('Ctrl Pts',(117.778442262019,1.63529765651769,330.361575198724));
#38368=CARTESIAN_POINT('Ctrl Pts',(117.770695118714,1.50587682985473,330.315947300545));
#38369=CARTESIAN_POINT('Ctrl Pts',(117.762947975408,1.37454584102702,330.275740457684));
#38370=CARTESIAN_POINT('Ctrl Pts',(117.755200832102,1.24179962063643,330.241101307583));
#38371=CARTESIAN_POINT('Ctrl Pts',(117.747451947074,1.10902355607731,330.206454369866));
#38372=CARTESIAN_POINT('Ctrl Pts',(117.739703062046,0.974832004960463,330.177377714394));
#38373=CARTESIAN_POINT('Ctrl Pts',(117.731954177018,0.839731911174272,330.15396725353));
#38374=CARTESIAN_POINT('Ctrl Pts',(117.724197067243,0.70448842075237,330.130531944562));
#38375=CARTESIAN_POINT('Ctrl Pts',(117.716439957468,0.568334847051531,330.112774910888));
#38376=CARTESIAN_POINT('Ctrl Pts',(117.708682847694,0.431785665005347,330.100740443496));
#38377=CARTESIAN_POINT('Ctrl Pts',(117.700921592768,0.295163515442321,330.08869954527));
#38378=CARTESIAN_POINT('Ctrl Pts',(117.693160337841,0.15814572656161,330.082387324559));
#38379=CARTESIAN_POINT('Ctrl Pts',(117.685399082915,0.0212476469387261,
330.081795896875));
#38380=CARTESIAN_POINT('Ctrl Pts',(117.677625412511,-0.115869424996714,
330.081203523099));
#38381=CARTESIAN_POINT('Ctrl Pts',(117.669851742106,-0.252866014204814,
330.086350214885));
#38382=CARTESIAN_POINT('Ctrl Pts',(117.662078071701,-0.389230127248695,
330.097176020849));
#38383=CARTESIAN_POINT('Ctrl Pts',(117.654666267524,-0.519246458023034,
330.10749788294));
#38384=CARTESIAN_POINT('Ctrl Pts',(117.647254463347,-0.648687585267904,
330.122981998134));
#38385=CARTESIAN_POINT('Ctrl Pts',(117.63984265917,-0.777119487138416,330.143533345609));
#38386=CARTESIAN_POINT('Ctrl Pts',(117.632067580392,-0.911846219098311,
330.165091975843));
#38387=CARTESIAN_POINT('Ctrl Pts',(117.624292501613,-1.04588805531016,330.19229524749));
#38388=CARTESIAN_POINT('Ctrl Pts',(117.616517422835,-1.17873482916488,330.225089816027));
#38389=CARTESIAN_POINT('Ctrl Pts',(117.608751911786,-1.31141812660662,330.257844028759));
#38390=CARTESIAN_POINT('Ctrl Pts',(117.600986400737,-1.44290891190943,330.296175755481));
#38391=CARTESIAN_POINT('Ctrl Pts',(117.593220889688,-1.57270400274552,330.339980130702));
#38392=CARTESIAN_POINT('Ctrl Pts',(117.585463078166,-1.70237040137199,330.383741073759));
#38393=CARTESIAN_POINT('Ctrl Pts',(117.577705266643,-1.83034408342,330.432963742791));
#38394=CARTESIAN_POINT('Ctrl Pts',(117.569947455121,-1.95613424791927,330.487492729467));
#38395=CARTESIAN_POINT('Ctrl Pts',(117.562195481598,-2.08182975132995,330.54198068135));
#38396=CARTESIAN_POINT('Ctrl Pts',(117.554443508075,-2.20534465064975,330.601766847826));
#38397=CARTESIAN_POINT('Ctrl Pts',(117.546691534552,-2.3262057876686,330.666646830004));
#38398=CARTESIAN_POINT('Ctrl Pts',(117.538942843994,-2.44701573992453,330.73149933547));
#38399=CARTESIAN_POINT('Ctrl Pts',(117.531194153437,-2.56517382150425,330.801441181563));
#38400=CARTESIAN_POINT('Ctrl Pts',(117.523445462879,-2.6802294607188,330.876221017029));
#38401=CARTESIAN_POINT('Ctrl Pts',(117.515698384501,-2.79526116164669,330.950985293925));
#38402=CARTESIAN_POINT('Ctrl Pts',(117.507951306124,-2.90719137660424,331.030585345153));
#38403=CARTESIAN_POINT('Ctrl Pts',(117.500204227746,-3.01559697654182,331.114725500358));
#38404=CARTESIAN_POINT('Ctrl Pts',(117.49245708444,-3.12400348502271,331.198866360738));
#38405=CARTESIAN_POINT('Ctrl Pts',(117.484709941134,-3.22888501078524,331.287547161327));
#38406=CARTESIAN_POINT('Ctrl Pts',(117.476962797828,-3.32985040792915,331.380431058356));
#38407=CARTESIAN_POINT('Ctrl Pts',(117.4692139128,-3.4308385042377,331.473335837657));
#38408=CARTESIAN_POINT('Ctrl Pts',(117.461465027772,-3.52790843236624,331.570445329149));
#38409=CARTESIAN_POINT('Ctrl Pts',(117.453716142744,-3.6207052011363,331.671385136582));
#38410=CARTESIAN_POINT('Ctrl Pts',(117.445959032969,-3.71360046535553,331.772432082571));
#38411=CARTESIAN_POINT('Ctrl Pts',(117.438201923195,-3.8022132450217,331.877317177585));
#38412=CARTESIAN_POINT('Ctrl Pts',(117.43044481342,-3.88622788299097,331.985631757074));
#38413=CARTESIAN_POINT('Ctrl Pts',(117.422683558494,-3.97028741569659,332.09400421641));
#38414=CARTESIAN_POINT('Ctrl Pts',(117.414922303568,-4.04974368440043,332.205809493404));
#38415=CARTESIAN_POINT('Ctrl Pts',(117.407161048642,-4.12432443465167,332.320609953696));
#38416=CARTESIAN_POINT('Ctrl Pts',(117.399387378237,-4.19902448979746,332.43559405731));
#38417=CARTESIAN_POINT('Ctrl Pts',(117.391613707832,-4.26883324215789,332.553582582111));
#38418=CARTESIAN_POINT('Ctrl Pts',(117.383840037428,-4.33352403710379,332.674112538762));
#38419=CARTESIAN_POINT('Ctrl Pts',(117.37642823325,-4.39520345998145,332.789031796933));
#38420=CARTESIAN_POINT('Ctrl Pts',(117.369016429073,-4.45223055845808,332.906260945549));
#38421=CARTESIAN_POINT('Ctrl Pts',(117.361604624896,-4.50445036344607,333.025383585161));
#38422=CARTESIAN_POINT('Ctrl Pts',(117.353031950123,-4.56484907261539,333.163163756249));
#38423=CARTESIAN_POINT('Ctrl Pts',(117.344459275349,-4.61898103881594,333.303850835865));
#38424=CARTESIAN_POINT('Ctrl Pts',(117.335886600575,-4.66658497031551,333.446884493244));
#38425=CARTESIAN_POINT('Ctrl Pts',(117.327347485539,-4.71400254510683,333.589358211965));
#38426=CARTESIAN_POINT('Ctrl Pts',(117.318808370503,-4.75494297021422,333.734159945722));
#38427=CARTESIAN_POINT('Ctrl Pts',(117.310269255467,-4.78919382292977,333.88071201699));
#38428=CARTESIAN_POINT('Ctrl Pts',(117.301751804726,-4.82335777898218,334.026892276026));
#38429=CARTESIAN_POINT('Ctrl Pts',(117.293234353986,-4.85086593947895,334.174813772444));
#38430=CARTESIAN_POINT('Ctrl Pts',(117.284716903245,-4.87155504716373,334.323882787563));
#38431=CARTESIAN_POINT('Ctrl Pts',(117.276233683062,-4.89216100794231,334.472352713171));
#38432=CARTESIAN_POINT('Ctrl Pts',(117.267750462878,-4.90600251753535,334.6219607101));
#38433=CARTESIAN_POINT('Ctrl Pts',(117.259267242695,-4.9129671501702,334.772103436076));
#38434=CARTESIAN_POINT('Ctrl Pts',(117.255023577975,-4.91645115331497,334.847211163488));
#38435=CARTESIAN_POINT('Ctrl Pts',(117.250779913256,-4.91821504616872,334.922452462763));
#38436=CARTESIAN_POINT('Ctrl Pts',(117.246536248536,-4.9182494855724,334.997750518554));
#38437=CARTESIAN_POINT('',(120.746536248543,-4.91824835509349,335.00402245201));
#38438=CARTESIAN_POINT('Ctrl Pts',(120.74653624849,-4.91824835509272,335.004022452949));
#38439=CARTESIAN_POINT('Ctrl Pts',(120.734143493174,-4.91806986260446,335.222265002467));
#38440=CARTESIAN_POINT('Ctrl Pts',(120.721750737859,-4.90336218246484,335.439931562694));
#38441=CARTESIAN_POINT('Ctrl Pts',(120.709357982543,-4.87436982771678,335.655516472062));
#38442=CARTESIAN_POINT('Ctrl Pts',(120.706392333757,-4.86743181115095,335.707107027073));
#38443=CARTESIAN_POINT('Ctrl Pts',(120.70342668497,-4.85967592412588,335.758578543016));
#38444=CARTESIAN_POINT('Ctrl Pts',(120.700461036184,-4.85110583398809,335.809910643186));
#38445=CARTESIAN_POINT('Ctrl Pts',(120.692685957405,-4.82863752072631,335.944488656775));
#38446=CARTESIAN_POINT('Ctrl Pts',(120.684910878627,-4.80052932182094,336.078343656673));
#38447=CARTESIAN_POINT('Ctrl Pts',(120.677135799848,-4.76683802711673,336.210965848294));
#38448=CARTESIAN_POINT('Ctrl Pts',(120.669370288799,-4.73318819169556,336.343424839865));
#38449=CARTESIAN_POINT('Ctrl Pts',(120.66160477775,-4.6939690258323,336.474653666432));
#38450=CARTESIAN_POINT('Ctrl Pts',(120.653839266701,-4.64928879197929,336.604149865591));
#38451=CARTESIAN_POINT('Ctrl Pts',(120.646081455179,-4.60465285870828,336.733517668892));
#38452=CARTESIAN_POINT('Ctrl Pts',(120.638323643657,-4.55456675960404,336.861155896394));
#38453=CARTESIAN_POINT('Ctrl Pts',(120.630565832134,-4.49918921516278,336.986574808222));
#38454=CARTESIAN_POINT('Ctrl Pts',(120.622813858611,-4.44385334407982,337.111899338342));
#38455=CARTESIAN_POINT('Ctrl Pts',(120.615061885088,-4.38323411084305,337.23500752092));
#38456=CARTESIAN_POINT('Ctrl Pts',(120.607309911565,-4.31753910620023,337.355427589405));
#38457=CARTESIAN_POINT('Ctrl Pts',(120.599561221008,-4.25187192343088,337.47579665992));
#38458=CARTESIAN_POINT('Ctrl Pts',(120.59181253045,-4.1811334314492,337.593479538154));
#38459=CARTESIAN_POINT('Ctrl Pts',(120.584063839892,-4.1055780197045,337.708027360759));
#38460=CARTESIAN_POINT('Ctrl Pts',(120.576316761515,-4.03003832789429,337.822551350732));
#38461=CARTESIAN_POINT('Ctrl Pts',(120.568569683137,-3.94968392485187,337.933941256413));
#38462=CARTESIAN_POINT('Ctrl Pts',(120.560822604759,-3.86481333272204,338.041775955871));
#38463=CARTESIAN_POINT('Ctrl Pts',(120.553075461453,-3.77994202929487,338.149611559087));
#38464=CARTESIAN_POINT('Ctrl Pts',(120.545328318147,-3.69055470302849,338.253891589497));
#38465=CARTESIAN_POINT('Ctrl Pts',(120.537581174841,-3.59699083247381,338.354227185746));
#38466=CARTESIAN_POINT('Ctrl Pts',(120.529832289813,-3.50340592677465,338.454585339567));
#38467=CARTESIAN_POINT('Ctrl Pts',(120.522083404785,-3.40564287485283,338.550997008797));
#38468=CARTESIAN_POINT('Ctrl Pts',(120.514334519757,-3.30407846263076,338.64310973967));
#38469=CARTESIAN_POINT('Ctrl Pts',(120.506577409982,-3.20240624889218,338.735320239948));
#38470=CARTESIAN_POINT('Ctrl Pts',(120.498820300208,-3.09692490494641,338.82322242397));
#38471=CARTESIAN_POINT('Ctrl Pts',(120.491063190433,-2.98804521850892,338.906503402615));
#38472=CARTESIAN_POINT('Ctrl Pts',(120.483301935507,-2.87910735024845,338.989828883953));
#38473=CARTESIAN_POINT('Ctrl Pts',(120.475540680581,-2.76676784099327,339.068528015209));
#38474=CARTESIAN_POINT('Ctrl Pts',(120.467779425654,-2.65146615438967,339.142331504675));
#38475=CARTESIAN_POINT('Ctrl Pts',(120.46000575525,-2.53598002266411,339.216253055673));
#38476=CARTESIAN_POINT('Ctrl Pts',(120.452232084845,-2.41752258254548,339.285263118501));
#38477=CARTESIAN_POINT('Ctrl Pts',(120.44445841444,-2.2965583440195,339.349138171525));
#38478=CARTESIAN_POINT('Ctrl Pts',(120.437046610263,-2.18122501989955,339.410039825463));
#38479=CARTESIAN_POINT('Ctrl Pts',(120.429634806086,-2.06361328781059,339.466273656212));
#38480=CARTESIAN_POINT('Ctrl Pts',(120.422223001909,-1.94414058462504,339.517687511295));
#38481=CARTESIAN_POINT('Ctrl Pts',(120.414447923131,-1.81881216836524,339.57162131257));
#38482=CARTESIAN_POINT('Ctrl Pts',(120.406672844352,-1.69103968400412,339.620421149492));
#38483=CARTESIAN_POINT('Ctrl Pts',(120.398897765574,-1.56128256092932,339.663858898749));
#38484=CARTESIAN_POINT('Ctrl Pts',(120.391132254525,-1.43168511225526,339.70724319509));
#38485=CARTESIAN_POINT('Ctrl Pts',(120.383366743476,-1.300108251307,339.745278409775));
#38486=CARTESIAN_POINT('Ctrl Pts',(120.375601232427,-1.16703309646476,339.777783671773));
#38487=CARTESIAN_POINT('Ctrl Pts',(120.367843420905,-1.03408988602594,339.810256704708));
#38488=CARTESIAN_POINT('Ctrl Pts',(120.360085609382,-0.899651715311847,
339.837210604213));
#38489=CARTESIAN_POINT('Ctrl Pts',(120.35232779786,-0.764216309800422,339.85851381539));
#38490=CARTESIAN_POINT('Ctrl Pts',(120.344575824337,-0.628882823726594,
339.879800995225));
#38491=CARTESIAN_POINT('Ctrl Pts',(120.336823850814,-0.492553981163142,
339.895445890281));
#38492=CARTESIAN_POINT('Ctrl Pts',(120.329071877291,-0.35573883993393,339.905367768095));
#38493=CARTESIAN_POINT('Ctrl Pts',(120.321323186733,-0.218981639998256,
339.915285443987));
#38494=CARTESIAN_POINT('Ctrl Pts',(120.313574496176,-0.0817389400515719,
339.919484894995));
#38495=CARTESIAN_POINT('Ctrl Pts',(120.305825805618,0.0554741364109582,
339.917937136919));
#38496=CARTESIAN_POINT('Ctrl Pts',(120.29807872724,0.192658664546857,339.916389700867));
#38497=CARTESIAN_POINT('Ctrl Pts',(120.290331648863,0.329813190854032,339.909097438578));
#38498=CARTESIAN_POINT('Ctrl Pts',(120.282584570485,0.466422037455538,339.896083490452));
#38499=CARTESIAN_POINT('Ctrl Pts',(120.274837427179,0.603032028970757,339.883069433256));
#38500=CARTESIAN_POINT('Ctrl Pts',(120.267090283873,0.739095942545852,339.864333631646));
#38501=CARTESIAN_POINT('Ctrl Pts',(120.259343140567,0.874103065048431,339.839951125184));
#38502=CARTESIAN_POINT('Ctrl Pts',(120.251594255539,1.00914054001834,339.815563137018));
#38503=CARTESIAN_POINT('Ctrl Pts',(120.243845370511,1.14312036656365,339.785525987294));
#38504=CARTESIAN_POINT('Ctrl Pts',(120.236096485483,1.27554225831209,339.749965790378));
#38505=CARTESIAN_POINT('Ctrl Pts',(120.228339375708,1.40810470402469,339.714367849501));
#38506=CARTESIAN_POINT('Ctrl Pts',(120.220582265934,1.53910553360685,339.673235252632));
#38507=CARTESIAN_POINT('Ctrl Pts',(120.212825156159,1.66805933111811,339.626744117667));
#38508=CARTESIAN_POINT('Ctrl Pts',(120.205063901233,1.79708203741562,339.580228139327));
#38509=CARTESIAN_POINT('Ctrl Pts',(120.197302646307,1.92405517035841,339.528348065013));
#38510=CARTESIAN_POINT('Ctrl Pts',(120.18954139138,2.04851445781022,339.471327719888));
#38511=CARTESIAN_POINT('Ctrl Pts',(120.181767720976,2.17317283956069,339.414216160794));
#38512=CARTESIAN_POINT('Ctrl Pts',(120.173994050571,2.29530899159242,339.351948077013));
#38513=CARTESIAN_POINT('Ctrl Pts',(120.166220380166,2.41448357678769,339.284793124519));
#38514=CARTESIAN_POINT('Ctrl Pts',(120.158808575989,2.52811055637085,339.220764251219));
#38515=CARTESIAN_POINT('Ctrl Pts',(120.151396771812,2.63904524113767,339.152293389084));
#38516=CARTESIAN_POINT('Ctrl Pts',(120.143984967635,2.74693378378046,339.079649231248));
#38517=CARTESIAN_POINT('Ctrl Pts',(120.136209888857,2.86011026528116,339.003444566842));
#38518=CARTESIAN_POINT('Ctrl Pts',(120.128434810078,2.9702921121187,338.922406350728));
#38519=CARTESIAN_POINT('Ctrl Pts',(120.1206597313,3.07703886693046,338.836797476268));
#38520=CARTESIAN_POINT('Ctrl Pts',(120.112894220251,3.18365426306458,338.751293948978));
#38521=CARTESIAN_POINT('Ctrl Pts',(120.105128709202,3.28684267587705,338.661231196664));
#38522=CARTESIAN_POINT('Ctrl Pts',(120.097363198153,3.38619164629601,338.566915922342));
#38523=CARTESIAN_POINT('Ctrl Pts',(120.089605386631,3.48544211192153,338.472694161888));
#38524=CARTESIAN_POINT('Ctrl Pts',(120.081847575109,3.5808604292853,338.374228537659));
#38525=CARTESIAN_POINT('Ctrl Pts',(120.074089763586,3.67206662325238,338.271866405723));
#38526=CARTESIAN_POINT('Ctrl Pts',(120.066337790063,3.76320418166611,338.169581304537));
#38527=CARTESIAN_POINT('Ctrl Pts',(120.05858581654,3.8501356669462,338.063405822796));
#38528=CARTESIAN_POINT('Ctrl Pts',(120.050833843017,3.93251770904395,337.953724349115));
#38529=CARTESIAN_POINT('Ctrl Pts',(120.04308515246,4.01486486229801,337.844089325604));
#38530=CARTESIAN_POINT('Ctrl Pts',(120.035336461902,4.09266617016763,337.730951575179));
#38531=CARTESIAN_POINT('Ctrl Pts',(120.027587771345,4.16561849634008,337.614728591164));
#38532=CARTESIAN_POINT('Ctrl Pts',(120.019840692967,4.23855564417176,337.498529788311));
#38533=CARTESIAN_POINT('Ctrl Pts',(120.012093614589,4.30664560934917,337.379247359521));
#38534=CARTESIAN_POINT('Ctrl Pts',(120.004346536211,4.3696287882395,337.257327471921));
#38535=CARTESIAN_POINT('Ctrl Pts',(119.996599392905,4.43261249498949,337.135406562514));
#38536=CARTESIAN_POINT('Ctrl Pts',(119.9888522496,4.49048915068558,337.010848497481));
#38537=CARTESIAN_POINT('Ctrl Pts',(119.981105106294,4.54304548151737,336.884123354604));
#38538=CARTESIAN_POINT('Ctrl Pts',(119.973356221266,4.59561362812812,336.757369721224));
#38539=CARTESIAN_POINT('Ctrl Pts',(119.965607336238,4.64285892001542,336.628448401501));
#38540=CARTESIAN_POINT('Ctrl Pts',(119.95785845121,4.68461667577673,336.497848344638));
#38541=CARTESIAN_POINT('Ctrl Pts',(119.950101341435,4.72641875365148,336.367109667525));
#38542=CARTESIAN_POINT('Ctrl Pts',(119.94234423166,4.76272154113165,336.234689066795));
#38543=CARTESIAN_POINT('Ctrl Pts',(119.934587121886,4.79341045309562,336.101090046569));
#38544=CARTESIAN_POINT('Ctrl Pts',(119.926825866959,4.82411576423291,335.967419635298));
#38545=CARTESIAN_POINT('Ctrl Pts',(119.919064612033,4.84920115088203,335.832569933865));
#38546=CARTESIAN_POINT('Ctrl Pts',(119.911303357107,4.86860358810352,335.69705248325));
#38547=CARTESIAN_POINT('Ctrl Pts',(119.903529686702,4.88803706290132,335.56131824888));
#38548=CARTESIAN_POINT('Ctrl Pts',(119.895756016298,4.90176938285342,335.4249145199));
#38549=CARTESIAN_POINT('Ctrl Pts',(119.887982345893,4.9097895568984,335.288356670586));
#38550=CARTESIAN_POINT('Ctrl Pts',(119.880570541716,4.91743638991207,335.158155622011));
#38551=CARTESIAN_POINT('Ctrl Pts',(119.873158737539,4.91989090453877,335.027814766544));
#38552=CARTESIAN_POINT('Ctrl Pts',(119.865746933362,4.91718756348704,334.897777067209));
#38553=CARTESIAN_POINT('Ctrl Pts',(119.857971854583,4.91435172363754,334.761365832868));
#38554=CARTESIAN_POINT('Ctrl Pts',(119.850196775805,4.90583067839006,334.624857138524));
#38555=CARTESIAN_POINT('Ctrl Pts',(119.842421697027,4.89160714362751,334.488763640855));
#38556=CARTESIAN_POINT('Ctrl Pts',(119.834656185978,4.87740111182999,334.352837614898));
#38557=CARTESIAN_POINT('Ctrl Pts',(119.826890674929,4.85750659312705,334.217326154058));
#38558=CARTESIAN_POINT('Ctrl Pts',(119.81912516388,4.83195829535756,334.08274207857));
#38559=CARTESIAN_POINT('Ctrl Pts',(119.811367352357,4.80643532879969,333.948291443585));
#38560=CARTESIAN_POINT('Ctrl Pts',(119.803609540835,4.77526981134047,333.814766745626));
#38561=CARTESIAN_POINT('Ctrl Pts',(119.795851729313,4.7385482157608,333.682675488192));
#38562=CARTESIAN_POINT('Ctrl Pts',(119.78809975579,4.70185425434634,333.550683633618));
#38563=CARTESIAN_POINT('Ctrl Pts',(119.780347782267,4.65961264140815,333.420123447526));
#38564=CARTESIAN_POINT('Ctrl Pts',(119.772595808744,4.61196080029828,333.291491691852));
#38565=CARTESIAN_POINT('Ctrl Pts',(119.764847118186,4.56432913977141,333.162914411802));
#38566=CARTESIAN_POINT('Ctrl Pts',(119.757098427629,4.51129194367738,333.036264303599));
#38567=CARTESIAN_POINT('Ctrl Pts',(119.749349737071,4.4530362466058,332.912022210627));
#38568=CARTESIAN_POINT('Ctrl Pts',(119.741602658693,4.39479267011855,332.78780596726));
#38569=CARTESIAN_POINT('Ctrl Pts',(119.733855580315,4.33133291812902,332.665997096264));
#38570=CARTESIAN_POINT('Ctrl Pts',(119.726108501938,4.2628916956706,332.547055350506));
#38571=CARTESIAN_POINT('Ctrl Pts',(119.718361358632,4.19444989960887,332.428112607901));
#38572=CARTESIAN_POINT('Ctrl Pts',(119.710614215326,4.12102674475167,332.312037377252));
#38573=CARTESIAN_POINT('Ctrl Pts',(119.70286707202,4.04290211483849,332.199263391118));
#38574=CARTESIAN_POINT('Ctrl Pts',(119.695118186992,3.96475992084993,332.086464050997));
#38575=CARTESIAN_POINT('Ctrl Pts',(119.687369301964,3.88191437105357,331.976967753509));
#38576=CARTESIAN_POINT('Ctrl Pts',(119.679620416936,3.79468751470903,331.871177581228));
#38577=CARTESIAN_POINT('Ctrl Pts',(119.671863307161,3.70736807487786,331.765275122165));
#38578=CARTESIAN_POINT('Ctrl Pts',(119.664106197386,3.61565828801369,331.66308694834));
#38579=CARTESIAN_POINT('Ctrl Pts',(119.656349087612,3.51991955288857,331.564981891796));
#38580=CARTESIAN_POINT('Ctrl Pts',(119.648587832686,3.42412965804449,331.466824411046));
#38581=CARTESIAN_POINT('Ctrl Pts',(119.640826577759,3.32430680933164,331.372754663119));
#38582=CARTESIAN_POINT('Ctrl Pts',(119.633065322833,3.22084706606405,331.28310247121));
#38583=CARTESIAN_POINT('Ctrl Pts',(119.625291652429,3.11722182092475,331.193306865011));
#38584=CARTESIAN_POINT('Ctrl Pts',(119.617517982024,3.00994836146576,331.107943179601));
#38585=CARTESIAN_POINT('Ctrl Pts',(119.609744311619,2.89945412901684,331.027299556193));
#38586=CARTESIAN_POINT('Ctrl Pts',(119.602332507442,2.79410342967243,330.950409912856));
#38587=CARTESIAN_POINT('Ctrl Pts',(119.594920703265,2.6858253023157,330.877810943292));
#38588=CARTESIAN_POINT('Ctrl Pts',(119.587508899088,2.57501089375246,330.809713379785));
#38589=CARTESIAN_POINT('Ctrl Pts',(119.57973382031,2.45876514092566,330.738278151837));
#38590=CARTESIAN_POINT('Ctrl Pts',(119.571958741531,2.33936084104629,330.671570993198));
#38591=CARTESIAN_POINT('Ctrl Pts',(119.564183662753,2.21721974462194,330.609883866393));
#38592=CARTESIAN_POINT('Ctrl Pts',(119.556418151704,2.09522895059262,330.548272649525));
#38593=CARTESIAN_POINT('Ctrl Pts',(119.548652640655,1.9705084065453,330.491669347627));
#38594=CARTESIAN_POINT('Ctrl Pts',(119.540887129606,1.84350813635811,330.440322290591));
#38595=CARTESIAN_POINT('Ctrl Pts',(119.533129318084,1.71663378730865,330.389026144312));
#38596=CARTESIAN_POINT('Ctrl Pts',(119.525371506561,1.58748457039647,330.342976017119));
#38597=CARTESIAN_POINT('Ctrl Pts',(119.517613695039,1.45653405152368,330.302373831471));
#38598=CARTESIAN_POINT('Ctrl Pts',(119.509861721516,1.32568207706911,330.261802200254));
#38599=CARTESIAN_POINT('Ctrl Pts',(119.502109747993,1.19303187062088,330.226670465523));
#38600=CARTESIAN_POINT('Ctrl Pts',(119.49435777447,1.05907553754994,330.197131891436));
#38601=CARTESIAN_POINT('Ctrl Pts',(119.486609083912,0.925175935065453,330.167605826952));
#38602=CARTESIAN_POINT('Ctrl Pts',(119.478860393355,0.789971687035495,330.143668295916));
#38603=CARTESIAN_POINT('Ctrl Pts',(119.471111702797,0.653968360069763,330.125422228897));
#38604=CARTESIAN_POINT('Ctrl Pts',(119.463364624419,0.517993329732128,330.107179958125));
#38605=CARTESIAN_POINT('Ctrl Pts',(119.455617546042,0.38121993831201,330.09462684794));
#38606=CARTESIAN_POINT('Ctrl Pts',(119.447870467664,0.24416181416412,330.087814328529));
#38607=CARTESIAN_POINT('Ctrl Pts',(119.440123324358,0.107102541337231,330.081001752022));
#38608=CARTESIAN_POINT('Ctrl Pts',(119.432376181052,-0.0302410785848208,
330.079929881657));
#38609=CARTESIAN_POINT('Ctrl Pts',(119.424629037746,-0.167352849489318,
330.084598074799));
#38610=CARTESIAN_POINT('Ctrl Pts',(119.416880152718,-0.30449544603088,330.089267317451));
#38611=CARTESIAN_POINT('Ctrl Pts',(119.40913126769,-0.441405699261192,330.09967917824));
#38612=CARTESIAN_POINT('Ctrl Pts',(119.401382382662,-0.577570369110589,
330.115780970183));
#38613=CARTESIAN_POINT('Ctrl Pts',(119.393625272887,-0.713879565547455,
330.131899852735));
#38614=CARTESIAN_POINT('Ctrl Pts',(119.385868163113,-0.849441208984974,
330.153720684638));
#38615=CARTESIAN_POINT('Ctrl Pts',(119.378111053338,-0.983749567076295,
330.181139154138));
#38616=CARTESIAN_POINT('Ctrl Pts',(119.370349798412,-1.11812969525979,330.208572275192));
#38617=CARTESIAN_POINT('Ctrl Pts',(119.362588543485,-1.25125482445359,330.241608899978));
#38618=CARTESIAN_POINT('Ctrl Pts',(119.354827288559,-1.38263326887683,330.280094460024));
#38619=CARTESIAN_POINT('Ctrl Pts',(119.347053618155,-1.51422187599501,330.318641584424));
#38620=CARTESIAN_POINT('Ctrl Pts',(119.33927994775,-1.64405784447323,330.36265493672));
#38621=CARTESIAN_POINT('Ctrl Pts',(119.331506277345,-1.77166755718988,330.411931002121));
#38622=CARTESIAN_POINT('Ctrl Pts',(119.324094473168,-1.89333700707897,330.458913254822));
#38623=CARTESIAN_POINT('Ctrl Pts',(119.316682668991,-2.01298253712763,330.510679173971));
#38624=CARTESIAN_POINT('Ctrl Pts',(119.309270864814,-2.13021526608317,330.567013875203));
#38625=CARTESIAN_POINT('Ctrl Pts',(119.301495786035,-2.25319392030266,330.626109707954));
#38626=CARTESIAN_POINT('Ctrl Pts',(119.293720707257,-2.37390591121925,330.690420259906));
#38627=CARTESIAN_POINT('Ctrl Pts',(119.285945628478,-2.49187748791643,330.759748869735));
#38628=CARTESIAN_POINT('Ctrl Pts',(119.278180117429,-2.60970389307808,330.828992166295));
#38629=CARTESIAN_POINT('Ctrl Pts',(119.27041460638,-2.72479626006984,330.903241038027));
#38630=CARTESIAN_POINT('Ctrl Pts',(119.262649095331,-2.83670222924492,330.982251435804));
#38631=CARTESIAN_POINT('Ctrl Pts',(119.254891283809,-2.94849724332576,331.061183494542));
#38632=CARTESIAN_POINT('Ctrl Pts',(119.247133472287,-3.05711182957005,331.144867460142));
#38633=CARTESIAN_POINT('Ctrl Pts',(119.239375660765,-3.16211991339303,331.233014372761));
#38634=CARTESIAN_POINT('Ctrl Pts',(119.231623687242,-3.26704897530287,331.321094952034));
#38635=CARTESIAN_POINT('Ctrl Pts',(119.223871713719,-3.36837663871759,331.413631543083));
#38636=CARTESIAN_POINT('Ctrl Pts',(119.216119740196,-3.46570771408276,331.510293264034));
#38637=CARTESIAN_POINT('Ctrl Pts',(119.208371049638,-3.56299756967973,331.606914048689));
#38638=CARTESIAN_POINT('Ctrl Pts',(119.20062235908,-3.65629392683993,331.707656213734));
#38639=CARTESIAN_POINT('Ctrl Pts',(119.192873668523,-3.74523663794914,331.812150319061));
#38640=CARTESIAN_POINT('Ctrl Pts',(119.185126590145,-3.83416084378441,331.916622683516));
#38641=CARTESIAN_POINT('Ctrl Pts',(119.177379511767,-3.91873295210075,332.024845138075));
#38642=CARTESIAN_POINT('Ctrl Pts',(119.169632433389,-3.99863176038211,332.136413593522));
#38643=CARTESIAN_POINT('Ctrl Pts',(119.161885290083,-4.07853123829235,332.247982984021));
#38644=CARTESIAN_POINT('Ctrl Pts',(119.154138146778,-4.15375711046519,332.362898113552));
#38645=CARTESIAN_POINT('Ctrl Pts',(119.146391003472,-4.22403057396825,332.480724554027));
#38646=CARTESIAN_POINT('Ctrl Pts',(119.138642118444,-4.29431983643781,332.598577484388));
#38647=CARTESIAN_POINT('Ctrl Pts',(119.130893233416,-4.35965427450441,332.719342692487));
#38648=CARTESIAN_POINT('Ctrl Pts',(119.123144348387,-4.41980045012489,332.84256007185));
#38649=CARTESIAN_POINT('Ctrl Pts',(119.115387238613,-4.48001046551765,332.965908235413));
#38650=CARTESIAN_POINT('Ctrl Pts',(119.107630128838,-4.53502104623235,333.091713417683));
#38651=CARTESIAN_POINT('Ctrl Pts',(119.099873019063,-4.58464622945744,333.219493888463));
#38652=CARTESIAN_POINT('Ctrl Pts',(119.092111764137,-4.63429793079373,333.347342641041));
#38653=CARTESIAN_POINT('Ctrl Pts',(119.084350509211,-4.67855837433095,333.477168415593));
#38654=CARTESIAN_POINT('Ctrl Pts',(119.076589254285,-4.71729146060522,333.608474097186));
#38655=CARTESIAN_POINT('Ctrl Pts',(119.06881558388,-4.75608650719445,333.739989825079));
#38656=CARTESIAN_POINT('Ctrl Pts',(119.061041913475,-4.78933643279507,333.872989811314));
#38657=CARTESIAN_POINT('Ctrl Pts',(119.053268243071,-4.8169560759355,334.006965647619));
#38658=CARTESIAN_POINT('Ctrl Pts',(119.045856438894,-4.84329001804257,334.134704876511));
#38659=CARTESIAN_POINT('Ctrl Pts',(119.038444634717,-4.8645060138211,334.263330864432));
#38660=CARTESIAN_POINT('Ctrl Pts',(119.03103283054,-4.88057431815725,334.39240030658));
#38661=CARTESIAN_POINT('Ctrl Pts',(119.019533969856,-4.90550309238889,334.592641907449));
#38662=CARTESIAN_POINT('Ctrl Pts',(119.008035109173,-4.91811212521678,334.794448535063));
#38663=CARTESIAN_POINT('Ctrl Pts',(118.99653624849,-4.91824887548693,334.996674151001));
#38664=CARTESIAN_POINT('',(122.496536248438,-4.9182498524359,335.001204788044));
#38665=CARTESIAN_POINT('Ctrl Pts',(122.496536248438,-4.9182498524359,335.001204788045));
#38666=CARTESIAN_POINT('Ctrl Pts',(122.488252845916,-4.91821382984681,335.148258117707));
#38667=CARTESIAN_POINT('Ctrl Pts',(122.479969443393,-4.91157834180379,335.295134724896));
#38668=CARTESIAN_POINT('Ctrl Pts',(122.471686040871,-4.89841612088684,335.441251140662));
#38669=CARTESIAN_POINT('Ctrl Pts',(122.463202974284,-4.88493663631842,335.590889562927));
#38670=CARTESIAN_POINT('Ctrl Pts',(122.454719907697,-4.86461188669965,335.739730340687));
#38671=CARTESIAN_POINT('Ctrl Pts',(122.44623684111,-4.83757469627169,335.887160707252));
#38672=CARTESIAN_POINT('Ctrl Pts',(122.437909913463,-4.8110351511475,336.031877477161));
#38673=CARTESIAN_POINT('Ctrl Pts',(122.429582985816,-4.77802828235813,336.175235047038));
#38674=CARTESIAN_POINT('Ctrl Pts',(122.421256058168,-4.73872973127174,336.31667140793));
#38675=CARTESIAN_POINT('Ctrl Pts',(122.412694922111,-4.69832584439482,336.462085896959));
#38676=CARTESIAN_POINT('Ctrl Pts',(122.404133786055,-4.65127130310775,336.605469186264));
#38677=CARTESIAN_POINT('Ctrl Pts',(122.395572649998,-4.59780918123002,336.746234175446));
#38678=CARTESIAN_POINT('Ctrl Pts',(122.387011513941,-4.54434705935229,336.886999164629));
#38679=CARTESIAN_POINT('Ctrl Pts',(122.378450377884,-4.48447755795471,337.025145573085));
#38680=CARTESIAN_POINT('Ctrl Pts',(122.369889241827,-4.4184938428861,337.160114631884));
#38681=CARTESIAN_POINT('Ctrl Pts',(122.362114163048,-4.35856855033833,337.282691245294));
#38682=CARTESIAN_POINT('Ctrl Pts',(122.35433908427,-4.29344397051479,337.402966017987));
#38683=CARTESIAN_POINT('Ctrl Pts',(122.346564005492,-4.22331996077631,337.520466538443));
#38684=CARTESIAN_POINT('Ctrl Pts',(122.338798494443,-4.15328224309601,337.637822467028));
#38685=CARTESIAN_POINT('Ctrl Pts',(122.331032983394,-4.07825753484646,337.75241060361));
#38686=CARTESIAN_POINT('Ctrl Pts',(122.323267472345,-3.99849293559624,337.86378024759));
#38687=CARTESIAN_POINT('Ctrl Pts',(122.315509660822,-3.91880742317863,337.975039468244));
#38688=CARTESIAN_POINT('Ctrl Pts',(122.3077518493,-3.8343915983921,338.083086231125));
#38689=CARTESIAN_POINT('Ctrl Pts',(122.299994037778,-3.74553729292212,338.187496423501));
#38690=CARTESIAN_POINT('Ctrl Pts',(122.292242064255,-3.65674985313468,338.291828043896));
#38691=CARTESIAN_POINT('Ctrl Pts',(122.284490090732,-3.56353083326843,338.392528244447));
#38692=CARTESIAN_POINT('Ctrl Pts',(122.276738117209,-3.46621377743365,338.489204079963));
#38693=CARTESIAN_POINT('Ctrl Pts',(122.268989426651,-3.36893793542969,338.585838973204));
#38694=CARTESIAN_POINT('Ctrl Pts',(122.261240736094,-3.26756778601032,338.678452616282));
#38695=CARTESIAN_POINT('Ctrl Pts',(122.253492045536,-3.16247519390871,338.766687365632));
#38696=CARTESIAN_POINT('Ctrl Pts',(122.245744967158,-3.05740446719868,338.854903757005));
#38697=CARTESIAN_POINT('Ctrl Pts',(122.23799788878,-2.94861313747918,338.938742815646));
#38698=CARTESIAN_POINT('Ctrl Pts',(122.230250810403,-2.83650745469667,339.017886076278));
#38699=CARTESIAN_POINT('Ctrl Pts',(122.222503667097,-2.72440083236055,339.097030000207));
#38700=CARTESIAN_POINT('Ctrl Pts',(122.214756523791,-2.6089801208757,339.171477822202));
#38701=CARTESIAN_POINT('Ctrl Pts',(122.207009380485,-2.49068162192992,339.240953680563));
#38702=CARTESIAN_POINT('Ctrl Pts',(122.199260495457,-2.37235652697011,339.310445158572));
#38703=CARTESIAN_POINT('Ctrl Pts',(122.191511610429,-2.2511526940969,339.374962250738));
#38704=CARTESIAN_POINT('Ctrl Pts',(122.183762725401,-2.12753179632469,339.434274632691));
#38705=CARTESIAN_POINT('Ctrl Pts',(122.176005615626,-2.00377968605431,339.49364996942));
#38706=CARTESIAN_POINT('Ctrl Pts',(122.168248505851,-1.87760573903,339.547809391211));
#38707=CARTESIAN_POINT('Ctrl Pts',(122.160491396077,-1.74949293076574,339.596570193927));
#38708=CARTESIAN_POINT('Ctrl Pts',(122.15273014115,-1.621311663113,339.645357052858));
#38709=CARTESIAN_POINT('Ctrl Pts',(122.144968886224,-1.49118984038717,339.688739420827));
#38710=CARTESIAN_POINT('Ctrl Pts',(122.137207631298,-1.35962548562458,339.726584559842));
#38711=CARTESIAN_POINT('Ctrl Pts',(122.129433960893,-1.22785067077109,339.764490238746));
#38712=CARTESIAN_POINT('Ctrl Pts',(122.121660290489,-1.09462909268573,339.79684089598));
#38713=CARTESIAN_POINT('Ctrl Pts',(122.113886620084,-0.960469723365517,
339.823554806675));
#38714=CARTESIAN_POINT('Ctrl Pts',(122.106474815907,-0.832555504965305,
339.8490251784));
#38715=CARTESIAN_POINT('Ctrl Pts',(122.09906301173,-0.703789123143303,339.8693717299));
#38716=CARTESIAN_POINT('Ctrl Pts',(122.091651207553,-0.574614073533863,
339.884567711579));
#38717=CARTESIAN_POINT('Ctrl Pts',(122.083876128775,-0.43910776994924,339.900508493586));
#38718=CARTESIAN_POINT('Ctrl Pts',(122.076101049996,-0.302723500652418,
339.91083142591));
#38719=CARTESIAN_POINT('Ctrl Pts',(122.068325971218,-0.165966680853271,
339.915448923887));
#38720=CARTESIAN_POINT('Ctrl Pts',(122.060560460169,-0.0293781490272524,
339.92006073974));
#38721=CARTESIAN_POINT('Ctrl Pts',(122.05279494912,0.107581634205588,339.918981077761));
#38722=CARTESIAN_POINT('Ctrl Pts',(122.045029438071,0.244399945341746,339.912173829296));
#38723=CARTESIAN_POINT('Ctrl Pts',(122.037271626548,0.381082600724122,339.905373330236));
#38724=CARTESIAN_POINT('Ctrl Pts',(122.029513815026,0.517623675278446,339.892856565358));
#38725=CARTESIAN_POINT('Ctrl Pts',(122.021756003504,0.653508596689846,339.874639430415));
#38726=CARTESIAN_POINT('Ctrl Pts',(122.014004029981,0.789291260388541,339.856436004443));
#38727=CARTESIAN_POINT('Ctrl Pts',(122.006252056458,0.924418367932922,339.832540798592));
#38728=CARTESIAN_POINT('Ctrl Pts',(121.998500082935,1.05837898346981,339.803021652028));
#38729=CARTESIAN_POINT('Ctrl Pts',(121.990751392377,1.19228286660657,339.77351500684));
#38730=CARTESIAN_POINT('Ctrl Pts',(121.98300270182,1.32502085936485,339.738389241995));
#38731=CARTESIAN_POINT('Ctrl Pts',(121.975254011262,1.45609097429646,339.697763525027));
#38732=CARTESIAN_POINT('Ctrl Pts',(121.967506932884,1.58713381899593,339.657146260578));
#38733=CARTESIAN_POINT('Ctrl Pts',(121.959759854507,1.71650910299104,339.611031435771));
#38734=CARTESIAN_POINT('Ctrl Pts',(121.952012776129,1.84372917688055,339.559588335017));
#38735=CARTESIAN_POINT('Ctrl Pts',(121.944265632823,1.97095031699678,339.50814480312));
#38736=CARTESIAN_POINT('Ctrl Pts',(121.936518489517,2.09601584861001,339.451373052736));
#38737=CARTESIAN_POINT('Ctrl Pts',(121.928771346211,2.21845768585406,339.389490694668));
#38738=CARTESIAN_POINT('Ctrl Pts',(121.921022461183,2.34092705062267,339.327594424132));
#38739=CARTESIAN_POINT('Ctrl Pts',(121.913273576155,2.46077119847885,339.260585435859));
#38740=CARTESIAN_POINT('Ctrl Pts',(121.905524691127,2.57754660698784,339.188727318805));
#38741=CARTESIAN_POINT('Ctrl Pts',(121.897767581352,2.6944459621219,339.116792930803));
#38742=CARTESIAN_POINT('Ctrl Pts',(121.890010471578,2.80826973794107,339.039999337746));
#38743=CARTESIAN_POINT('Ctrl Pts',(121.882253361803,2.91860292887465,338.958653812354));
#38744=CARTESIAN_POINT('Ctrl Pts',(121.874492106877,3.0289950783377,338.877264818514));
#38745=CARTESIAN_POINT('Ctrl Pts',(121.86673085195,3.13589262175083,338.791319290345));
#38746=CARTESIAN_POINT('Ctrl Pts',(121.858969597024,3.23891442806256,338.701164193897));
#38747=CARTESIAN_POINT('Ctrl Pts',(121.85119592662,3.34210103568965,338.610864878677));
#38748=CARTESIAN_POINT('Ctrl Pts',(121.843422256215,3.44139923368296,338.516342808417));
#38749=CARTESIAN_POINT('Ctrl Pts',(121.83564858581,3.53646486390482,338.417981762512));
#38750=CARTESIAN_POINT('Ctrl Pts',(121.828236781633,3.62710516616851,338.324199446958));
#38751=CARTESIAN_POINT('Ctrl Pts',(121.820824977456,3.71389789321751,338.226927735874));
#38752=CARTESIAN_POINT('Ctrl Pts',(121.813413173279,3.79658054981075,338.12652509846));
#38753=CARTESIAN_POINT('Ctrl Pts',(121.805638094501,3.88331572970239,338.021201428702));
#38754=CARTESIAN_POINT('Ctrl Pts',(121.797863015722,3.96580185756734,337.912099318029));
#38755=CARTESIAN_POINT('Ctrl Pts',(121.790087936944,4.04369177242485,337.799596383789));
#38756=CARTESIAN_POINT('Ctrl Pts',(121.782322425895,4.12148583878341,337.687231891572));
#38757=CARTESIAN_POINT('Ctrl Pts',(121.774556914846,4.19469472545002,337.571475220895));
#38758=CARTESIAN_POINT('Ctrl Pts',(121.766791403797,4.26301060377761,337.452737991425));
#38759=CARTESIAN_POINT('Ctrl Pts',(121.759033592274,4.33125874671298,337.334118490264));
#38760=CARTESIAN_POINT('Ctrl Pts',(121.751275780752,4.39462334225948,337.212524648007));
#38761=CARTESIAN_POINT('Ctrl Pts',(121.74351796923,4.45283929289114,337.088397781598));
#38762=CARTESIAN_POINT('Ctrl Pts',(121.735765995707,4.51101143417379,336.964364324592));
#38763=CARTESIAN_POINT('Ctrl Pts',(121.728014022184,4.56404247727582,336.837801990055));
#38764=CARTESIAN_POINT('Ctrl Pts',(121.720262048661,4.61171297289221,336.709177146512));
#38765=CARTESIAN_POINT('Ctrl Pts',(121.712513358103,4.65936328002541,336.580606775666));
#38766=CARTESIAN_POINT('Ctrl Pts',(121.704764667546,4.70165741937806,336.449975998841));
#38767=CARTESIAN_POINT('Ctrl Pts',(121.697015976988,4.73842394725883,336.317771436382));
#38768=CARTESIAN_POINT('Ctrl Pts',(121.68926889861,4.7751828255564,336.185594380186));
#38769=CARTESIAN_POINT('Ctrl Pts',(121.681521820233,4.80641627528101,336.051844566003));
#38770=CARTESIAN_POINT('Ctrl Pts',(121.673774741855,4.83200275623447,335.917023678125));
#38771=CARTESIAN_POINT('Ctrl Pts',(121.666027598549,4.85758945162727,335.782201660319));
#38772=CARTESIAN_POINT('Ctrl Pts',(121.658280455243,4.87752901097182,335.646308934934));
#38773=CARTESIAN_POINT('Ctrl Pts',(121.650533311937,4.89175111971402,335.509856887054));
#38774=CARTESIAN_POINT('Ctrl Pts',(121.642784426909,4.9059764258882,335.373374161857));
#38775=CARTESIAN_POINT('Ctrl Pts',(121.635035541881,4.91448168313653,335.236332252633));
#38776=CARTESIAN_POINT('Ctrl Pts',(121.627286656853,4.91724853359589,335.099246769968));
#38777=CARTESIAN_POINT('Ctrl Pts',(121.619529547078,4.92001832081892,334.962015783355));
#38778=CARTESIAN_POINT('Ctrl Pts',(121.611772437304,4.91703752640005,334.824741522326));
#38779=CARTESIAN_POINT('Ctrl Pts',(121.604015327529,4.90833995919861,334.68793925682));
#38780=CARTESIAN_POINT('Ctrl Pts',(121.596254072603,4.89963774429536,334.551063888557));
#38781=CARTESIAN_POINT('Ctrl Pts',(121.588492817677,4.88521271061089,334.414661406896));
#38782=CARTESIAN_POINT('Ctrl Pts',(121.58073156275,4.86515037741903,334.279240076309));
#38783=CARTESIAN_POINT('Ctrl Pts',(121.572957892346,4.84505595103237,334.143602115726));
#38784=CARTESIAN_POINT('Ctrl Pts',(121.565184221941,4.81930627827437,334.008948826707));
#38785=CARTESIAN_POINT('Ctrl Pts',(121.557410551536,4.78803784370988,333.875777304222));
#38786=CARTESIAN_POINT('Ctrl Pts',(121.549998747359,4.75822496229697,333.748804948148));
#38787=CARTESIAN_POINT('Ctrl Pts',(121.542586943182,4.72339563001726,333.623179788013));
#38788=CARTESIAN_POINT('Ctrl Pts',(121.535175139005,4.68370924003127,333.499316549919));
#38789=CARTESIAN_POINT('Ctrl Pts',(121.527400060227,4.64207770185253,333.369382405557));
#38790=CARTESIAN_POINT('Ctrl Pts',(121.519624981448,4.59496938623718,333.240976648509));
#38791=CARTESIAN_POINT('Ctrl Pts',(121.51184990267,4.54251397094156,333.114595564262));
#38792=CARTESIAN_POINT('Ctrl Pts',(121.504084391621,4.49012310537392,332.988369999985));
#38793=CARTESIAN_POINT('Ctrl Pts',(121.496318880572,4.43239838074171,332.864164508724));
#38794=CARTESIAN_POINT('Ctrl Pts',(121.488553369523,4.36951935306018,332.742460701176));
#38795=CARTESIAN_POINT('Ctrl Pts',(121.480795558,4.30670267011765,332.620877563308));
#38796=CARTESIAN_POINT('Ctrl Pts',(121.473037746478,4.23874203258317,332.50179151799));
#38797=CARTESIAN_POINT('Ctrl Pts',(121.465279934956,4.1658650938064,332.385664313309));
#38798=CARTESIAN_POINT('Ctrl Pts',(121.457527961433,4.09304299723716,332.269624498032));
#38799=CARTESIAN_POINT('Ctrl Pts',(121.44977598791,4.01531217037886,332.156539421157));
#38800=CARTESIAN_POINT('Ctrl Pts',(121.442024014387,3.9329460358628,332.046846001054));
#38801=CARTESIAN_POINT('Ctrl Pts',(121.434275323829,3.85061478345361,331.93719903618));
#38802=CARTESIAN_POINT('Ctrl Pts',(121.426526633272,3.76365236197711,331.83094118316));
#38803=CARTESIAN_POINT('Ctrl Pts',(121.418777942714,3.67237520284385,331.728479950843));
#38804=CARTESIAN_POINT('Ctrl Pts',(121.411030864336,3.58111703468588,331.626040036441));
#38805=CARTESIAN_POINT('Ctrl Pts',(121.403283785958,3.48554617433257,331.527395463213));
#38806=CARTESIAN_POINT('Ctrl Pts',(121.395536707581,3.38601872643472,331.432919927065));
#38807=CARTESIAN_POINT('Ctrl Pts',(121.387789564275,3.28649044440102,331.33844359912));
#38808=CARTESIAN_POINT('Ctrl Pts',(121.380042420969,3.1830057921737,331.248136647046));
#38809=CARTESIAN_POINT('Ctrl Pts',(121.372295277663,3.07595675313919,331.162334939665));
#38810=CARTESIAN_POINT('Ctrl Pts',(121.364546392635,2.96888364720807,331.076513942238));
#38811=CARTESIAN_POINT('Ctrl Pts',(121.356797507607,2.85824486480913,330.995200449422));
#38812=CARTESIAN_POINT('Ctrl Pts',(121.349048622579,2.74446405939093,330.918688925209));
#38813=CARTESIAN_POINT('Ctrl Pts',(121.341291512804,2.63056248585021,330.842096190874));
#38814=CARTESIAN_POINT('Ctrl Pts',(121.333534403029,2.5135125522349,330.770315825055));
#38815=CARTESIAN_POINT('Ctrl Pts',(121.325777293255,2.39376585594316,330.703598239291));
#38816=CARTESIAN_POINT('Ctrl Pts',(121.318016038328,2.27395517084569,330.636845001783));
#38817=CARTESIAN_POINT('Ctrl Pts',(121.310254783402,2.15144520056255,330.575160110753));
#38818=CARTESIAN_POINT('Ctrl Pts',(121.302493528476,2.02670963491755,330.518746702291));
#38819=CARTESIAN_POINT('Ctrl Pts',(121.294719858071,1.90177453301879,330.462243050759));
#38820=CARTESIAN_POINT('Ctrl Pts',(121.286946187667,1.77460708413481,330.411027878834));
#38821=CARTESIAN_POINT('Ctrl Pts',(121.279172517262,1.6456991656623,330.365255420345));
#38822=CARTESIAN_POINT('Ctrl Pts',(121.271760713085,1.52279194180933,330.321613680812));
#38823=CARTESIAN_POINT('Ctrl Pts',(121.264348908908,1.39830291435526,330.282919426859));
#38824=CARTESIAN_POINT('Ctrl Pts',(121.256937104731,1.27266709211144,330.249263053467));
#38825=CARTESIAN_POINT('Ctrl Pts',(121.249162025953,1.14087348396843,330.213957080957));
#38826=CARTESIAN_POINT('Ctrl Pts',(121.241386947174,1.00740133079538,330.18408374551));
#38827=CARTESIAN_POINT('Ctrl Pts',(121.233611868396,0.87273814572275,330.159802566888));
#38828=CARTESIAN_POINT('Ctrl Pts',(121.225846357347,0.738240672272432,330.135551267803));
#38829=CARTESIAN_POINT('Ctrl Pts',(121.218080846298,0.602555464120857,330.116878502018));
#38830=CARTESIAN_POINT('Ctrl Pts',(121.210315335249,0.466184686040631,330.103893904234));
#38831=CARTESIAN_POINT('Ctrl Pts',(121.202557523727,0.329949119983904,330.090922180715));
#38832=CARTESIAN_POINT('Ctrl Pts',(121.194799712204,0.19302972333652,330.083627438418));
#38833=CARTESIAN_POINT('Ctrl Pts',(121.187041900682,0.0559379862049669,
330.082068117166));
#38834=CARTESIAN_POINT('Ctrl Pts',(121.179289927159,-0.0810505850469661,
330.080509969352));
#38835=CARTESIAN_POINT('Ctrl Pts',(121.171537953636,-0.218210849362863,
330.084678656054));
#38836=CARTESIAN_POINT('Ctrl Pts',(121.163785980113,-0.355027428088145,
330.094580691948));
#38837=CARTESIAN_POINT('Ctrl Pts',(121.156037289555,-0.491786064911109,
330.104478534325));
#38838=CARTESIAN_POINT('Ctrl Pts',(121.148288598998,-0.628200916591018,
330.120104868463));
#38839=CARTESIAN_POINT('Ctrl Pts',(121.14053990844,-0.763758061050371,330.14141412686));
#38840=CARTESIAN_POINT('Ctrl Pts',(121.132792830062,-0.899287001713625,
330.162718951687));
#38841=CARTESIAN_POINT('Ctrl Pts',(121.125045751684,-1.03395820422216,330.189704288275));
#38842=CARTESIAN_POINT('Ctrl Pts',(121.117298673307,-1.16726471105814,330.222272908922));
#38843=CARTESIAN_POINT('Ctrl Pts',(121.109551530001,-1.30057233513105,330.254841802526));
#38844=CARTESIAN_POINT('Ctrl Pts',(121.101804386695,-1.43251486101219,330.292993980753));
#38845=CARTESIAN_POINT('Ctrl Pts',(121.094057243389,-1.56259772474264,330.336581574303));
#38846=CARTESIAN_POINT('Ctrl Pts',(121.086308358361,-1.69270983386246,330.38017896727));
#38847=CARTESIAN_POINT('Ctrl Pts',(121.078559473333,-1.82096107832683,330.429214083034));
#38848=CARTESIAN_POINT('Ctrl Pts',(121.070810588305,-1.94687457389216,330.483490013735));
#38849=CARTESIAN_POINT('Ctrl Pts',(121.06305347853,-2.07292171534266,330.53782355347));
#38850=CARTESIAN_POINT('Ctrl Pts',(121.055296368755,-2.1966257917297,330.597408865097));
#38851=CARTESIAN_POINT('Ctrl Pts',(121.047539258981,-2.317531841383,330.662001702781));
#38852=CARTESIAN_POINT('Ctrl Pts',(121.039778004055,-2.43850249936338,330.726629056812));
#38853=CARTESIAN_POINT('Ctrl Pts',(121.032016749128,-2.55667181476036,330.796269070445));
#38854=CARTESIAN_POINT('Ctrl Pts',(121.024255494202,-2.67161262535982,330.870633336392));
#38855=CARTESIAN_POINT('Ctrl Pts',(121.016481823798,-2.78673730379719,330.94511656093));
#38856=CARTESIAN_POINT('Ctrl Pts',(121.008708153393,-2.8986228379547,331.02433891344));
#38857=CARTESIAN_POINT('Ctrl Pts',(121.000934482988,-3.00687334623065,331.107970228502));
#38858=CARTESIAN_POINT('Ctrl Pts',(120.993522678811,-3.11008476730356,331.187708485728));
#38859=CARTESIAN_POINT('Ctrl Pts',(120.986110874634,-3.20999174689452,331.271454283682));
#38860=CARTESIAN_POINT('Ctrl Pts',(120.978699070457,-3.30628286170681,331.358890732087));
#38861=CARTESIAN_POINT('Ctrl Pts',(120.971039942796,-3.40578710161219,331.449244835427));
#38862=CARTESIAN_POINT('Ctrl Pts',(120.963380815135,-3.50176462688324,331.543844415688));
#38863=CARTESIAN_POINT('Ctrl Pts',(120.955721687474,-3.59382317637695,331.642379110228));
#38864=CARTESIAN_POINT('Ctrl Pts',(120.948072075932,-3.68576734729001,331.74079137987));
#38865=CARTESIAN_POINT('Ctrl Pts',(120.94042246439,-3.7738019527125,331.843128749123));
#38866=CARTESIAN_POINT('Ctrl Pts',(120.932772852849,-3.85756823507023,331.949041072994));
#38867=CARTESIAN_POINT('Ctrl Pts',(120.925012994336,-3.94254176551617,332.056479815931));
#38868=CARTESIAN_POINT('Ctrl Pts',(120.917253135823,-4.02312265110909,332.167597105007));
#38869=CARTESIAN_POINT('Ctrl Pts',(120.90949327731,-4.09897502778376,332.281988450336));
#38870=CARTESIAN_POINT('Ctrl Pts',(120.901857084696,-4.17361857412897,332.394556784526));
#38871=CARTESIAN_POINT('Ctrl Pts',(120.894220892082,-4.24368296867924,332.510295247593));
#38872=CARTESIAN_POINT('Ctrl Pts',(120.886584699468,-4.30888915332716,332.628785685173));
#38873=CARTESIAN_POINT('Ctrl Pts',(120.878951511157,-4.37406968393813,332.747229505119));
#38874=CARTESIAN_POINT('Ctrl Pts',(120.871318322847,-4.43439561110258,332.868422793726));
#38875=CARTESIAN_POINT('Ctrl Pts',(120.863685134536,-4.48963242435178,332.991920380884));
#38876=CARTESIAN_POINT('Ctrl Pts',(120.856053182759,-4.5448602895486,333.115397962129));
#38877=CARTESIAN_POINT('Ctrl Pts',(120.848421230982,-4.59500051666463,333.241178730914));
#38878=CARTESIAN_POINT('Ctrl Pts',(120.840789279205,-4.63986583957253,333.368795520706));
#38879=CARTESIAN_POINT('Ctrl Pts',(120.832934859983,-4.68603896342454,333.500132273877));
#38880=CARTESIAN_POINT('Ctrl Pts',(120.825080440761,-4.72662478170577,333.633413309007));
#38881=CARTESIAN_POINT('Ctrl Pts',(120.817226021539,-4.76147380476872,333.768111097135));
#38882=CARTESIAN_POINT('Ctrl Pts',(120.809588196785,-4.79536182671955,333.89909444185));
#38883=CARTESIAN_POINT('Ctrl Pts',(120.801950372031,-4.82382525267203,334.031417014512));
#38884=CARTESIAN_POINT('Ctrl Pts',(120.794312547278,-4.84677845086613,334.164582912121));
#38885=CARTESIAN_POINT('Ctrl Pts',(120.786349830822,-4.87070801391076,334.303413314547));
#38886=CARTESIAN_POINT('Ctrl Pts',(120.778387114366,-4.88864816190976,334.443159882849));
#38887=CARTESIAN_POINT('Ctrl Pts',(120.77042439791,-4.90056191064571,334.583255447032));
#38888=CARTESIAN_POINT('Ctrl Pts',(120.762461681455,-4.91247565938166,334.723351011215));
#38889=CARTESIAN_POINT('Ctrl Pts',(120.754498964999,-4.91836304183632,334.863795077535));
#38890=CARTESIAN_POINT('Ctrl Pts',(120.746536248543,-4.91824835509349,335.00402245201));
#38891=CARTESIAN_POINT('',(124.246536248521,-4.91824792744739,334.995484841147));
#38892=CARTESIAN_POINT('Ctrl Pts',(124.24653624849,-4.91824792744789,334.995484841695));
#38893=CARTESIAN_POINT('Ctrl Pts',(124.238867278053,-4.91837231136742,335.130973104362));
#38894=CARTESIAN_POINT('Ctrl Pts',(124.231198307617,-4.91289382317161,335.266601363009));
#38895=CARTESIAN_POINT('Ctrl Pts',(124.22352933718,-4.90180460816653,335.401863964368));
#38896=CARTESIAN_POINT('Ctrl Pts',(124.215853841775,-4.89070595815681,335.537241650814));
#38897=CARTESIAN_POINT('Ctrl Pts',(124.208178346371,-4.87398701663746,335.672252655387));
#38898=CARTESIAN_POINT('Ctrl Pts',(124.200502850966,-4.85169222915224,335.806390461305));
#38899=CARTESIAN_POINT('Ctrl Pts',(124.192840454809,-4.82943549066893,335.940299343326));
#38900=CARTESIAN_POINT('Ctrl Pts',(124.185178058652,-4.80162198093284,336.073337607823));
#38901=CARTESIAN_POINT('Ctrl Pts',(124.177515662495,-4.76834765888175,336.205007745426));
#38902=CARTESIAN_POINT('Ctrl Pts',(124.169853753625,-4.73507545289661,336.336669509525));
#38903=CARTESIAN_POINT('Ctrl Pts',(124.162191844755,-4.69634322324669,336.466962931612));
#38904=CARTESIAN_POINT('Ctrl Pts',(124.154529935884,-4.65229756023208,336.595402918876));
#38905=CARTESIAN_POINT('Ctrl Pts',(124.14686676733,-4.60824465572831,336.723864022789));
#38906=CARTESIAN_POINT('Ctrl Pts',(124.139203598775,-4.55887671063673,336.850470707267));
#38907=CARTESIAN_POINT('Ctrl Pts',(124.13154043022,-4.50438929995784,336.974755705632));
#38908=CARTESIAN_POINT('Ctrl Pts',(124.123855181658,-4.44974489384719,337.099398808313));
#38909=CARTESIAN_POINT('Ctrl Pts',(124.116169933095,-4.38995164429082,337.221706458019));
#38910=CARTESIAN_POINT('Ctrl Pts',(124.108484684533,-4.3252537414127,337.341231115225));
#38911=CARTESIAN_POINT('Ctrl Pts',(124.100809883398,-4.26064378971032,337.460593289047));
#38912=CARTESIAN_POINT('Ctrl Pts',(124.093135082263,-4.19114275147848,337.577179708469));
#38913=CARTESIAN_POINT('Ctrl Pts',(124.085460281128,-4.1170374390443,337.690573505409));
#38914=CARTESIAN_POINT('Ctrl Pts',(124.077769808852,-4.04278081131301,337.804198840622));
#38915=CARTESIAN_POINT('Ctrl Pts',(124.070079336575,-3.96390134438794,337.914618191908));
#38916=CARTESIAN_POINT('Ctrl Pts',(124.062388864299,-3.8807277299219,338.021445903655));
#38917=CARTESIAN_POINT('Ctrl Pts',(124.054698392023,-3.7975541154559,338.128273615403));
#38918=CARTESIAN_POINT('Ctrl Pts',(124.047007919747,-3.71008665864779,338.231509425653));
#38919=CARTESIAN_POINT('Ctrl Pts',(124.039317447471,-3.61868988274723,338.330805697576));
#38920=CARTESIAN_POINT('Ctrl Pts',(124.031542368692,-3.52628760793234,338.431194374483));
#38921=CARTESIAN_POINT('Ctrl Pts',(124.023767289914,-3.42955872278655,338.52789367449));
#38922=CARTESIAN_POINT('Ctrl Pts',(124.015992211135,-3.32882954335569,338.620507828162));
#38923=CARTESIAN_POINT('Ctrl Pts',(124.008226700086,-3.22822431759288,338.713008014222));
#38924=CARTESIAN_POINT('Ctrl Pts',(124.000461189037,-3.12362887712746,338.801432794272));
#38925=CARTESIAN_POINT('Ctrl Pts',(123.992695677988,-3.01540862382393,338.885420684285));
#38926=CARTESIAN_POINT('Ctrl Pts',(123.984937866466,-2.90729567121673,338.96932530006));
#38927=CARTESIAN_POINT('Ctrl Pts',(123.977180054944,-2.79556536486126,339.048801542328));
#38928=CARTESIAN_POINT('Ctrl Pts',(123.969422243422,-2.68061839541984,339.123526170723));
#38929=CARTESIAN_POINT('Ctrl Pts',(123.961670269899,-2.56575792721845,339.198194566465));
#38930=CARTESIAN_POINT('Ctrl Pts',(123.953918296376,-2.44768594049332,339.268118253486));
#38931=CARTESIAN_POINT('Ctrl Pts',(123.946166322853,-2.3268342140595,339.333015763043));
#38932=CARTESIAN_POINT('Ctrl Pts',(123.938417632295,-2.20603366840316,339.397885788467));
#38933=CARTESIAN_POINT('Ctrl Pts',(123.930668941738,-2.08245606809512,339.457733685502));
#38934=CARTESIAN_POINT('Ctrl Pts',(123.92292025118,-1.95655984991967,339.512322751775));
#38935=CARTESIAN_POINT('Ctrl Pts',(123.915173172802,-1.83068982550396,339.566900460336));
#38936=CARTESIAN_POINT('Ctrl Pts',(123.907426094424,-1.70250250115246,339.616221359065));
#38937=CARTESIAN_POINT('Ctrl Pts',(123.899679016047,-1.57247809385156,339.660096104895));
#38938=CARTESIAN_POINT('Ctrl Pts',(123.891931872741,-1.44245259682079,339.703971218438));
#38939=CARTESIAN_POINT('Ctrl Pts',(123.884184729435,-1.3105903564888,339.74239996307));
#38940=CARTESIAN_POINT('Ctrl Pts',(123.876437586129,-1.17738823951595,339.7752424018));
#38941=CARTESIAN_POINT('Ctrl Pts',(123.868688701101,-1.04415617587965,339.808092224208));
#38942=CARTESIAN_POINT('Ctrl Pts',(123.860939816073,-0.909584015617764,
339.835353148018));
#38943=CARTESIAN_POINT('Ctrl Pts',(123.853190931045,-0.774179952228243,
339.856936119002));
#38944=CARTESIAN_POINT('Ctrl Pts',(123.84543382127,-0.638632169566438,339.878541998374));
#38945=CARTESIAN_POINT('Ctrl Pts',(123.837676711495,-0.502251106531569,
339.894457824521));
#38946=CARTESIAN_POINT('Ctrl Pts',(123.829919601721,-0.36555178951698,339.904646261626));
#38947=CARTESIAN_POINT('Ctrl Pts',(123.822158346795,-0.228779424758129,
339.914840143106));
#38948=CARTESIAN_POINT('Ctrl Pts',(123.814397091868,-0.0916888576196233,
339.919300524453));
#38949=CARTESIAN_POINT('Ctrl Pts',(123.806635836942,0.0452047168919196,
339.918042252367));
#38950=CARTESIAN_POINT('Ctrl Pts',(123.798862166538,0.182317276508983,339.916781967457));
#38951=CARTESIAN_POINT('Ctrl Pts',(123.791088496133,0.319231823217834,339.909784768699));
#38952=CARTESIAN_POINT('Ctrl Pts',(123.783314825728,0.455437220326082,339.897117519607));
#38953=CARTESIAN_POINT('Ctrl Pts',(123.775903021551,0.585302223430506,339.885039934008));
#38954=CARTESIAN_POINT('Ctrl Pts',(123.768491217374,0.714522327711021,339.867808338154));
#38955=CARTESIAN_POINT('Ctrl Pts',(123.761079413197,0.842664834777234,339.845523608314));
#38956=CARTESIAN_POINT('Ctrl Pts',(123.753304334418,0.977087987830924,339.822146637482));
#38957=CARTESIAN_POINT('Ctrl Pts',(123.74552925564,1.1107500422505,339.793134794181));
#38958=CARTESIAN_POINT('Ctrl Pts',(123.737754176862,1.24314159873856,339.758548310986));
#38959=CARTESIAN_POINT('Ctrl Pts',(123.729988665813,1.37537023898794,339.72400438866));
#38960=CARTESIAN_POINT('Ctrl Pts',(123.722223154764,1.50633111751356,339.683899573625));
#38961=CARTESIAN_POINT('Ctrl Pts',(123.714457643715,1.63552251476752,339.638345520354));
#38962=CARTESIAN_POINT('Ctrl Pts',(123.706699832192,1.76458581837474,339.59283663406));
#38963=CARTESIAN_POINT('Ctrl Pts',(123.69894202067,1.89188276590224,339.541889390821));
#38964=CARTESIAN_POINT('Ctrl Pts',(123.691184209148,2.01692470091968,339.485665816055));
#38965=CARTESIAN_POINT('Ctrl Pts',(123.683432235625,2.141872537916,339.429484551311));
#38966=CARTESIAN_POINT('Ctrl Pts',(123.675680262102,2.26456838507538,339.368035017985));
#38967=CARTESIAN_POINT('Ctrl Pts',(123.667928288579,2.38454188903436,339.301527989208));
#38968=CARTESIAN_POINT('Ctrl Pts',(123.660179598021,2.50446458414293,339.235049126197));
#38969=CARTESIAN_POINT('Ctrl Pts',(123.652430907464,2.62166688796647,339.163517216843));
#38970=CARTESIAN_POINT('Ctrl Pts',(123.644682216906,2.73570166597968,339.087189677181));
#38971=CARTESIAN_POINT('Ctrl Pts',(123.636935138528,2.84971271810498,339.010878018101));
#38972=CARTESIAN_POINT('Ctrl Pts',(123.629188060151,2.96055723065519,338.929772930632));
#38973=CARTESIAN_POINT('Ctrl Pts',(123.621440981773,3.06781610803996,338.844175775085));
#38974=CARTESIAN_POINT('Ctrl Pts',(123.613693838467,3.1750758843574,338.758577902151));
#38975=CARTESIAN_POINT('Ctrl Pts',(123.605946695161,3.27874966005724,338.66848812986));
#38976=CARTESIAN_POINT('Ctrl Pts',(123.598199551855,3.37845087607788,338.57424855605));
#38977=CARTESIAN_POINT('Ctrl Pts',(123.590450666827,3.4781745070483,338.479987795184));
#38978=CARTESIAN_POINT('Ctrl Pts',(123.582701781799,3.5739235171337,338.381575644755));
#38979=CARTESIAN_POINT('Ctrl Pts',(123.574952896771,3.66534800606997,338.279391263161));
#38980=CARTESIAN_POINT('Ctrl Pts',(123.567195786996,3.75686953390367,338.177098422009));
#38981=CARTESIAN_POINT('Ctrl Pts',(123.559438677222,3.84405711041111,338.071025643319));
#38982=CARTESIAN_POINT('Ctrl Pts',(123.551681567447,3.92660062877545,337.961585819219));
#38983=CARTESIAN_POINT('Ctrl Pts',(123.543920312521,4.00918825575675,337.852087513977));
#38984=CARTESIAN_POINT('Ctrl Pts',(123.536159057595,4.08712665772259,337.739218899655));
#38985=CARTESIAN_POINT('Ctrl Pts',(123.528397802668,4.16014951800182,337.623421249127));
#38986=CARTESIAN_POINT('Ctrl Pts',(123.520624132264,4.23328919105941,337.507438360096));
#38987=CARTESIAN_POINT('Ctrl Pts',(123.512850461859,4.3014974147242,337.388517411078));
#38988=CARTESIAN_POINT('Ctrl Pts',(123.505076791454,4.36455381055837,337.267124411505));
#38989=CARTESIAN_POINT('Ctrl Pts',(123.497664987277,4.42467491599633,337.151382285266));
#38990=CARTESIAN_POINT('Ctrl Pts',(123.4902531831,4.48011291249718,337.033393337522));
#38991=CARTESIAN_POINT('Ctrl Pts',(123.482841378923,4.53071847113989,336.913576023515));
#38992=CARTESIAN_POINT('Ctrl Pts',(123.475066300145,4.58380435895752,336.787886106033));
#38993=CARTESIAN_POINT('Ctrl Pts',(123.467291221366,4.63173988815878,336.659786859807));
#38994=CARTESIAN_POINT('Ctrl Pts',(123.459516142588,4.67430004441115,336.529739244877));
#38995=CARTESIAN_POINT('Ctrl Pts',(123.451750631539,4.71680782768174,336.399851661817));
#38996=CARTESIAN_POINT('Ctrl Pts',(123.44398512049,4.75395327902397,336.268020848508));
#38997=CARTESIAN_POINT('Ctrl Pts',(123.436219609441,4.78555878183027,336.134729134264));
#38998=CARTESIAN_POINT('Ctrl Pts',(123.428461797919,4.81713294768859,336.001569579142));
#38999=CARTESIAN_POINT('Ctrl Pts',(123.420703986396,4.84317800654216,335.866952383536));
#39000=CARTESIAN_POINT('Ctrl Pts',(123.412946174874,4.86356576898616,335.731376150313));
#39001=CARTESIAN_POINT('Ctrl Pts',(123.405194201351,4.88393818899236,335.595901942504));
#39002=CARTESIAN_POINT('Ctrl Pts',(123.397442227828,4.89866172863496,335.459470518571));
#39003=CARTESIAN_POINT('Ctrl Pts',(123.389690254305,4.90765909634135,335.322591470126));
#39004=CARTESIAN_POINT('Ctrl Pts',(123.381941563747,4.91665265365717,335.185770390039));
#39005=CARTESIAN_POINT('Ctrl Pts',(123.37419287319,4.91992483668058,335.048502451701));
#39006=CARTESIAN_POINT('Ctrl Pts',(123.366444182632,4.91745014189946,334.91130296266));
#39007=CARTESIAN_POINT('Ctrl Pts',(123.358697104254,4.91497596199927,334.774132019118));
#39008=CARTESIAN_POINT('Ctrl Pts',(123.350950025877,4.90675728964313,334.637029887112));
#39009=CARTESIAN_POINT('Ctrl Pts',(123.343202947499,4.89282074847415,334.500512076421));
#39010=CARTESIAN_POINT('Ctrl Pts',(123.335455804193,4.87888409050351,334.363993121579));
#39011=CARTESIAN_POINT('Ctrl Pts',(123.327708660887,4.85922950783392,334.228058886673));
#39012=CARTESIAN_POINT('Ctrl Pts',(123.319961517581,4.83393548854778,334.093219566235));
#39013=CARTESIAN_POINT('Ctrl Pts',(123.312212632553,4.80863578262904,333.958349931055));
#39014=CARTESIAN_POINT('Ctrl Pts',(123.304463747525,4.7776941892355,333.824576084272));
#39015=CARTESIAN_POINT('Ctrl Pts',(123.296714862497,4.74124019964471,333.69239744885));
#39016=CARTESIAN_POINT('Ctrl Pts',(123.288957752722,4.70474751741284,333.56007851766));
#39017=CARTESIAN_POINT('Ctrl Pts',(123.281200642947,4.66273085531849,333.429358557505));
#39018=CARTESIAN_POINT('Ctrl Pts',(123.273443533173,4.61536960656995,333.300721783447));
#39019=CARTESIAN_POINT('Ctrl Pts',(123.265682278247,4.56798304948439,333.172016270011));
#39020=CARTESIAN_POINT('Ctrl Pts',(123.25792102332,4.5152463651625,333.045396521445));
#39021=CARTESIAN_POINT('Ctrl Pts',(123.250159768394,4.45738651014688,332.921325287194));
#39022=CARTESIAN_POINT('Ctrl Pts',(123.24238609799,4.39943409821974,332.797055579402));
#39023=CARTESIAN_POINT('Ctrl Pts',(123.234612427585,4.33634231873491,332.675342879767));
#39024=CARTESIAN_POINT('Ctrl Pts',(123.22683875718,4.26838378954875,332.556624693663));
#39025=CARTESIAN_POINT('Ctrl Pts',(123.219426953003,4.2035887462465,332.443432867685));
#39026=CARTESIAN_POINT('Ctrl Pts',(123.212015148826,4.13437000384308,332.332963283882));
#39027=CARTESIAN_POINT('Ctrl Pts',(123.204603344649,4.06099863983351,332.225567966273));
#39028=CARTESIAN_POINT('Ctrl Pts',(123.196828265871,3.98403112671128,332.112908884233));
#39029=CARTESIAN_POINT('Ctrl Pts',(123.189053187092,3.90225040307346,332.003277022603));
#39030=CARTESIAN_POINT('Ctrl Pts',(123.181278108314,3.81592233188421,331.89711105266));
#39031=CARTESIAN_POINT('Ctrl Pts',(123.173512597265,3.72970049288233,331.791075726701));
#39032=CARTESIAN_POINT('Ctrl Pts',(123.165747086216,3.63894268461023,331.688498106672));
#39033=CARTESIAN_POINT('Ctrl Pts',(123.157981575167,3.54395838953981,331.589788570233));
#39034=CARTESIAN_POINT('Ctrl Pts',(123.150223763644,3.44906827167421,331.491176904587));
#39035=CARTESIAN_POINT('Ctrl Pts',(123.142465952122,3.34996027576758,331.396425970075));
#39036=CARTESIAN_POINT('Ctrl Pts',(123.1347081406,3.24698431696538,331.305913386522));
#39037=CARTESIAN_POINT('Ctrl Pts',(123.126956167077,3.14408585083783,331.215468916558));
#39038=CARTESIAN_POINT('Ctrl Pts',(123.119204193554,3.03732550795233,331.129256706036));
#39039=CARTESIAN_POINT('Ctrl Pts',(123.111452220031,2.92708998786247,331.047617520349));
#39040=CARTESIAN_POINT('Ctrl Pts',(123.103703529473,2.81690115258131,330.966012908906));
#39041=CARTESIAN_POINT('Ctrl Pts',(123.095954838916,2.70324038074115,330.888977702525));
#39042=CARTESIAN_POINT('Ctrl Pts',(123.088206148358,2.58652720403971,330.816812210137));
#39043=CARTESIAN_POINT('Ctrl Pts',(123.08045906998,2.46983831048941,330.744661732382));
#39044=CARTESIAN_POINT('Ctrl Pts',(123.072711991602,2.35009860754055,330.677379158757));
#39045=CARTESIAN_POINT('Ctrl Pts',(123.064964913224,2.22775600594537,330.615221072793));
#39046=CARTESIAN_POINT('Ctrl Pts',(123.057217769919,2.10541237900115,330.553062465886));
#39047=CARTESIAN_POINT('Ctrl Pts',(123.049470626613,1.98046615837642,330.496028609352));
#39048=CARTESIAN_POINT('Ctrl Pts',(123.041723483307,1.85338885194286,330.444329596427));
#39049=CARTESIAN_POINT('Ctrl Pts',(123.033974598279,1.72628297583324,330.392618960466));
#39050=CARTESIAN_POINT('Ctrl Pts',(123.026225713251,1.5970454225206,330.346245702025));
#39051=CARTESIAN_POINT('Ctrl Pts',(123.018476828223,1.46616624259004,330.305371195548));
#39052=CARTESIAN_POINT('Ctrl Pts',(123.010719718448,1.3351481461455,330.264453304448));
#39053=CARTESIAN_POINT('Ctrl Pts',(123.002962608673,1.20248531608825,330.22904594084));
#39054=CARTESIAN_POINT('Ctrl Pts',(122.995205498898,1.06868201915229,330.199260285702));
#39055=CARTESIAN_POINT('Ctrl Pts',(122.987444243972,0.93480722201275,330.169458714062));
#39056=CARTESIAN_POINT('Ctrl Pts',(122.979682989046,0.799791128213023,330.145284905607));
#39057=CARTESIAN_POINT('Ctrl Pts',(122.97192173412,0.664145692840228,330.126798428017));
#39058=CARTESIAN_POINT('Ctrl Pts',(122.964148063715,0.52828326897758,330.108282378086));
#39059=CARTESIAN_POINT('Ctrl Pts',(122.95637439331,0.391789881143109,330.095471875814));
#39060=CARTESIAN_POINT('Ctrl Pts',(122.948600722906,0.255180966104411,330.088374430289));
#39061=CARTESIAN_POINT('Ctrl Pts',(122.941188918729,0.124931228928863,330.081607372561));
#39062=CARTESIAN_POINT('Ctrl Pts',(122.933777114552,-0.00542323414057583,
330.080033459226));
#39063=CARTESIAN_POINT('Ctrl Pts',(122.926365310375,-0.135439703008916,
330.083615235831));
#39064=CARTESIAN_POINT('Ctrl Pts',(122.918590231596,-0.271828666317511,
330.087372565977));
#39065=CARTESIAN_POINT('Ctrl Pts',(122.910815152818,-0.408276679793586,
330.096815630196));
#39066=CARTESIAN_POINT('Ctrl Pts',(122.903040074039,-0.544270981694427,
330.11195824885));
#39067=CARTESIAN_POINT('Ctrl Pts',(122.89527456299,-0.680097933948819,330.127082233547));
#39068=CARTESIAN_POINT('Ctrl Pts',(122.887509051941,-0.815471900766772,
330.147891774656));
#39069=CARTESIAN_POINT('Ctrl Pts',(122.879743540892,-0.949880308093416,
330.174348700663));
#39070=CARTESIAN_POINT('Ctrl Pts',(122.87198572937,-1.0841554490931,330.20077939455));
#39071=CARTESIAN_POINT('Ctrl Pts',(122.864227917848,-1.21746655474758,330.232846255212));
#39072=CARTESIAN_POINT('Ctrl Pts',(122.856470106326,-1.34930671732538,330.270459383293));
#39073=CARTESIAN_POINT('Ctrl Pts',(122.848718132803,-1.48104766599924,330.308044206302));
#39074=CARTESIAN_POINT('Ctrl Pts',(122.84096615928,-1.6113195005258,330.351166882297));
#39075=CARTESIAN_POINT('Ctrl Pts',(122.833214185757,-1.73962639869795,330.399686635081));
#39076=CARTESIAN_POINT('Ctrl Pts',(122.825465495199,-1.86787895882302,330.448185839721));
#39077=CARTESIAN_POINT('Ctrl Pts',(122.817716804641,-1.99416787283916,330.502077437156));
#39078=CARTESIAN_POINT('Ctrl Pts',(122.809968114084,-2.11801357188558,330.561171148624));
#39079=CARTESIAN_POINT('Ctrl Pts',(122.802221035706,-2.24183350380001,330.620252565152));
#39080=CARTESIAN_POINT('Ctrl Pts',(122.794473957328,-2.36321087930042,330.684533774634));
#39081=CARTESIAN_POINT('Ctrl Pts',(122.78672687895,-2.4816875416116,330.753776971436));
#39082=CARTESIAN_POINT('Ctrl Pts',(122.778979735645,-2.60016519687084,330.823020748561));
#39083=CARTESIAN_POINT('Ctrl Pts',(122.771232592339,-2.71574175298579,330.897226398723));
#39084=CARTESIAN_POINT('Ctrl Pts',(122.763485449033,-2.82798537810988,330.976111114395));
#39085=CARTESIAN_POINT('Ctrl Pts',(122.755736564005,-2.94025423798401,331.055013565026));
#39086=CARTESIAN_POINT('Ctrl Pts',(122.747987678977,-3.04918835608372,331.138596949729));
#39087=CARTESIAN_POINT('Ctrl Pts',(122.740238793949,-3.15438683470517,331.226536503484));
#39088=CARTESIAN_POINT('Ctrl Pts',(122.732481684174,-3.25969697207885,331.31456939719));
#39089=CARTESIAN_POINT('Ctrl Pts',(122.724724574399,-3.36126324905533,331.4069674451));
#39090=CARTESIAN_POINT('Ctrl Pts',(122.716967464625,-3.4587192835137,331.503366764965));
#39091=CARTESIAN_POINT('Ctrl Pts',(122.709206209698,-3.55622739536091,331.599817597545));
#39092=CARTESIAN_POINT('Ctrl Pts',(122.701444954772,-3.6496206221926,331.700273676415));
#39093=CARTESIAN_POINT('Ctrl Pts',(122.693683699846,-3.73857182400419,331.80433672311));
#39094=CARTESIAN_POINT('Ctrl Pts',(122.685910029441,-3.82766531874958,331.908566236766));
#39095=CARTESIAN_POINT('Ctrl Pts',(122.678136359037,-3.912302347557,332.016413940708));
#39096=CARTESIAN_POINT('Ctrl Pts',(122.670362688632,-3.9921976634614,332.127450456763));
#39097=CARTESIAN_POINT('Ctrl Pts',(122.662950884455,-4.06837383318914,332.233318196282));
#39098=CARTESIAN_POINT('Ctrl Pts',(122.655539080278,-4.14023965019631,332.342084310452));
#39099=CARTESIAN_POINT('Ctrl Pts',(122.648127276101,-4.2075870294846,332.453356237749));
#39100=CARTESIAN_POINT('Ctrl Pts',(122.640098530856,-4.28054024550361,332.573890177372));
#39101=CARTESIAN_POINT('Ctrl Pts',(122.632069785611,-4.348409418628,332.697724738684));
#39102=CARTESIAN_POINT('Ctrl Pts',(122.624041040366,-4.41089340609883,332.824407569756));
#39103=CARTESIAN_POINT('Ctrl Pts',(122.616024308214,-4.47328390125301,332.950900850324));
#39104=CARTESIAN_POINT('Ctrl Pts',(122.608007576063,-4.53030510255302,333.080233596217));
#39105=CARTESIAN_POINT('Ctrl Pts',(122.599990843912,-4.58169993115081,333.211925951368));
#39106=CARTESIAN_POINT('Ctrl Pts',(122.591984868597,-4.63302579826329,333.343441601961));
#39107=CARTESIAN_POINT('Ctrl Pts',(122.583978893282,-4.67874020175239,333.47731022567));
#39108=CARTESIAN_POINT('Ctrl Pts',(122.575972917967,-4.71863265997295,333.613028881794));
#39109=CARTESIAN_POINT('Ctrl Pts',(122.567979254774,-4.7584637689112,333.748538820719));
#39110=CARTESIAN_POINT('Ctrl Pts',(122.559985591582,-4.79249068257633,333.885892779966));
#39111=CARTESIAN_POINT('Ctrl Pts',(122.551991928389,-4.82055175829656,334.024569936857));
#39112=CARTESIAN_POINT('Ctrl Pts',(122.544005574865,-4.84858717404663,334.163120282796));
#39113=CARTESIAN_POINT('Ctrl Pts',(122.536019221341,-4.87066754613693,334.302991069189));
#39114=CARTESIAN_POINT('Ctrl Pts',(122.528032867817,-4.88668140797001,334.443647701991));
#39115=CARTESIAN_POINT('Ctrl Pts',(122.520054174503,-4.90267990991051,334.584169422253));
#39116=CARTESIAN_POINT('Ctrl Pts',(122.512075481188,-4.91262346031404,334.725475133635));
#39117=CARTESIAN_POINT('Ctrl Pts',(122.504096787873,-4.91645195726336,334.867021752075));
#39118=CARTESIAN_POINT('Ctrl Pts',(122.501576608079,-4.91766124057254,334.911731194296));
#39119=CARTESIAN_POINT('Ctrl Pts',(122.499056428284,-4.91826081210291,334.956464617952));
#39120=CARTESIAN_POINT('Ctrl Pts',(122.49653624849,-4.91824985243613,335.001204787119));
#39121=CARTESIAN_POINT('',(125.996536248531,-4.91824989020686,335.001039220942));
#39122=CARTESIAN_POINT('Ctrl Pts',(125.99653624849,-4.91824989020671,335.001039221667));
#39123=CARTESIAN_POINT('Ctrl Pts',(125.993352061456,-4.91823808096415,335.056927977462));
#39124=CARTESIAN_POINT('Ctrl Pts',(125.990167874422,-4.91727366286132,335.112805554363));
#39125=CARTESIAN_POINT('Ctrl Pts',(125.986983687388,-4.91535758023749,335.168650291734));
#39126=CARTESIAN_POINT('Ctrl Pts',(125.97920860861,-4.91067893128005,335.305010759195));
#39127=CARTESIAN_POINT('Ctrl Pts',(125.971433529831,-4.90031427907279,335.441391864294));
#39128=CARTESIAN_POINT('Ctrl Pts',(125.963658451053,-4.88425326763991,335.577280763623));
#39129=CARTESIAN_POINT('Ctrl Pts',(125.955892940004,-4.86821202030407,335.71300244301));
#39130=CARTESIAN_POINT('Ctrl Pts',(125.948127428955,-4.84648840654108,335.848232737317));
#39131=CARTESIAN_POINT('Ctrl Pts',(125.940361917906,-4.81912405979518,335.982459342061));
#39132=CARTESIAN_POINT('Ctrl Pts',(125.932604106383,-4.79178684487883,336.116552860735));
#39133=CARTESIAN_POINT('Ctrl Pts',(125.924846294861,-4.7588201045514,336.249644289744));
#39134=CARTESIAN_POINT('Ctrl Pts',(125.917088483339,-4.72031716063909,336.381227340258));
#39135=CARTESIAN_POINT('Ctrl Pts',(125.909336509816,-4.68184319141301,336.512711370354));
#39136=CARTESIAN_POINT('Ctrl Pts',(125.901584536293,-4.63784142048731,336.642688907688));
#39137=CARTESIAN_POINT('Ctrl Pts',(125.89383256277,-4.58845597047808,336.770665092411));
#39138=CARTESIAN_POINT('Ctrl Pts',(125.886083872212,-4.53909143523628,336.898587079144));
#39139=CARTESIAN_POINT('Ctrl Pts',(125.878335181655,-4.48434789608241,337.024509035126));
#39140=CARTESIAN_POINT('Ctrl Pts',(125.870586491097,-4.42441886726431,337.147952687909));
#39141=CARTESIAN_POINT('Ctrl Pts',(125.862839412719,-4.36450230718121,337.271370657209));
#39142=CARTESIAN_POINT('Ctrl Pts',(125.855092334341,-4.2994025740111,337.39231099753));
#39143=CARTESIAN_POINT('Ctrl Pts',(125.847345255964,-4.22936056313782,337.510317169099));
#39144=CARTESIAN_POINT('Ctrl Pts',(125.839598112658,-4.15931796524507,337.628324329674));
#39145=CARTESIAN_POINT('Ctrl Pts',(125.831850969352,-4.08433320653738,337.743396936323));
#39146=CARTESIAN_POINT('Ctrl Pts',(125.824103826046,-4.0046920054174,337.855105077619));
#39147=CARTESIAN_POINT('Ctrl Pts',(125.816354941018,-3.9250328992646,337.966838333277));
#39148=CARTESIAN_POINT('Ctrl Pts',(125.80860605599,-3.84071549441394,338.075205300218));
#39149=CARTESIAN_POINT('Ctrl Pts',(125.800857170962,-3.75206725682389,338.179807283904));
#39150=CARTESIAN_POINT('Ctrl Pts',(125.793100061187,-3.66332492707852,338.284520293217));
#39151=CARTESIAN_POINT('Ctrl Pts',(125.785342951412,-3.57024283518527,338.385460037843));
#39152=CARTESIAN_POINT('Ctrl Pts',(125.777585841638,-3.47318733026035,338.482262602306));
#39153=CARTESIAN_POINT('Ctrl Pts',(125.769824586712,-3.3760799619769,338.579116894964));
#39154=CARTESIAN_POINT('Ctrl Pts',(125.762063331785,-3.27499523778071,338.671829338219));
#39155=CARTESIAN_POINT('Ctrl Pts',(125.754302076859,-3.17033363711312,338.760075490185));
#39156=CARTESIAN_POINT('Ctrl Pts',(125.746528406455,-3.06550461199349,338.848462807235));
#39157=CARTESIAN_POINT('Ctrl Pts',(125.73875473605,-2.95708758575487,338.932369316592));
#39158=CARTESIAN_POINT('Ctrl Pts',(125.730981065645,-2.84551385381968,339.011512678557));
#39159=CARTESIAN_POINT('Ctrl Pts',(125.723569261468,-2.73913390594905,339.086971897981));
#39160=CARTESIAN_POINT('Ctrl Pts',(125.716157457291,-2.62988476906911,339.158101282463));
#39161=CARTESIAN_POINT('Ctrl Pts',(125.708745653114,-2.51816040151034,339.224695403785));
#39162=CARTESIAN_POINT('Ctrl Pts',(125.700970574336,-2.40096008988791,339.294553501367));
#39163=CARTESIAN_POINT('Ctrl Pts',(125.693195495557,-2.280665401014,339.359641285721));
#39164=CARTESIAN_POINT('Ctrl Pts',(125.685420416779,-2.15770199163858,339.419672519291));
#39165=CARTESIAN_POINT('Ctrl Pts',(125.67765490573,-2.03488989656664,339.479629880607));
#39166=CARTESIAN_POINT('Ctrl Pts',(125.669889394681,-1.90941596316459,339.534542902102));
#39167=CARTESIAN_POINT('Ctrl Pts',(125.662123883632,-1.78173352944661,339.584169356879));
#39168=CARTESIAN_POINT('Ctrl Pts',(125.654366072109,-1.6541776932334,339.633746606881));
#39169=CARTESIAN_POINT('Ctrl Pts',(125.646608260587,-1.52441807637631,339.678047580646));
#39170=CARTESIAN_POINT('Ctrl Pts',(125.638850449065,-1.39293092974834,339.716876772553));
#39171=CARTESIAN_POINT('Ctrl Pts',(125.631098475542,-1.26154273136795,339.755676744262));
#39172=CARTESIAN_POINT('Ctrl Pts',(125.623346502019,-1.1284299642057,339.789013019915));
#39173=CARTESIAN_POINT('Ctrl Pts',(125.615594528496,-0.994086759483296,
339.816738998235));
#39174=CARTESIAN_POINT('Ctrl Pts',(125.607845837938,-0.859800449187851,
339.844453234588));
#39175=CARTESIAN_POINT('Ctrl Pts',(125.600097147381,-0.724285119755702,
339.866561820393));
#39176=CARTESIAN_POINT('Ctrl Pts',(125.592348456823,-0.588047682355619,
339.882968665246));
#39177=CARTESIAN_POINT('Ctrl Pts',(125.584601378445,-0.451838590292264,
339.899372096518));
#39178=CARTESIAN_POINT('Ctrl Pts',(125.576854300067,-0.314908076926829,
339.910076099757));
#39179=CARTESIAN_POINT('Ctrl Pts',(125.56910722169,-0.177770418609592,339.915036189162));
#39180=CARTESIAN_POINT('Ctrl Pts',(125.561360078384,-0.0406316109467381,
339.919996320137));
#39181=CARTESIAN_POINT('Ctrl Pts',(125.553612935078,0.0967139545117735,
339.919212427132));
#39182=CARTESIAN_POINT('Ctrl Pts',(125.545865791772,0.233750137453922,339.912692127107));
#39183=CARTESIAN_POINT('Ctrl Pts',(125.538116906744,0.370817129039309,339.90617036118));
#39184=CARTESIAN_POINT('Ctrl Pts',(125.530368021716,0.507574209343861,339.893909640515));
#39185=CARTESIAN_POINT('Ctrl Pts',(125.522619136688,0.643508897006027,339.875969581732));
#39186=CARTESIAN_POINT('Ctrl Pts',(125.514862026913,0.779587867150193,339.858010481185));
#39187=CARTESIAN_POINT('Ctrl Pts',(125.507104917139,0.914842312834073,339.834360052031));
#39188=CARTESIAN_POINT('Ctrl Pts',(125.499347807364,1.04876795724189,339.805129429512));
#39189=CARTESIAN_POINT('Ctrl Pts',(125.491586552438,1.18276516723197,339.775883187083));
#39190=CARTESIAN_POINT('Ctrl Pts',(125.483825297511,1.31543178320089,339.741050908843));
#39191=CARTESIAN_POINT('Ctrl Pts',(125.476064042585,1.44627825264097,339.700793792376));
#39192=CARTESIAN_POINT('Ctrl Pts',(125.468290372181,1.5773340337894,339.660472277642));
#39193=CARTESIAN_POINT('Ctrl Pts',(125.460516701776,1.70656348144028,339.61470871407));
#39194=CARTESIAN_POINT('Ctrl Pts',(125.452743031371,1.8334957714153,339.563712996969));
#39195=CARTESIAN_POINT('Ctrl Pts',(125.445331227194,1.95451933275402,339.515091142767));
#39196=CARTESIAN_POINT('Ctrl Pts',(125.437919423017,2.07345452632375,339.461713404183));
#39197=CARTESIAN_POINT('Ctrl Pts',(125.43050761884,2.18991540969609,339.403799900186));
#39198=CARTESIAN_POINT('Ctrl Pts',(125.422732540062,2.31208438788146,339.343047882842));
#39199=CARTESIAN_POINT('Ctrl Pts',(125.414957461283,2.43191645298921,339.277112247443));
#39200=CARTESIAN_POINT('Ctrl Pts',(125.407182382505,2.54894055446037,339.206196038266));
#39201=CARTESIAN_POINT('Ctrl Pts',(125.399416871456,2.66582065032452,339.135367096));
#39202=CARTESIAN_POINT('Ctrl Pts',(125.391651360407,2.77989932667487,339.059569975373));
#39203=CARTESIAN_POINT('Ctrl Pts',(125.383885849358,2.89072756253167,338.979054815119));
#39204=CARTESIAN_POINT('Ctrl Pts',(125.376128037835,3.00144591186995,338.898619485881));
#39205=CARTESIAN_POINT('Ctrl Pts',(125.368370226313,3.10891992011577,338.813475654659));
#39206=CARTESIAN_POINT('Ctrl Pts',(125.360612414791,3.21272745574601,338.723918011664));
#39207=CARTESIAN_POINT('Ctrl Pts',(125.352860441268,3.31645687291369,338.634427763635));
#39208=CARTESIAN_POINT('Ctrl Pts',(125.345108467745,3.41652501462897,338.540530569483));
#39209=CARTESIAN_POINT('Ctrl Pts',(125.337356494222,3.5125411979933,338.442562620331));
#39210=CARTESIAN_POINT('Ctrl Pts',(125.329607803664,3.60851671844701,338.344636160663));
#39211=CARTESIAN_POINT('Ctrl Pts',(125.321859113107,3.7004434205406,338.242642653421));
#39212=CARTESIAN_POINT('Ctrl Pts',(125.314110422549,3.78796618108195,338.136956370988));
#39213=CARTESIAN_POINT('Ctrl Pts',(125.306363344171,3.87547073178196,338.031292077468));
#39214=CARTESIAN_POINT('Ctrl Pts',(125.298616265794,3.95857291431835,337.921936837842));
#39215=CARTESIAN_POINT('Ctrl Pts',(125.290869187416,4.03695701519037,337.809299044247));
#39216=CARTESIAN_POINT('Ctrl Pts',(125.28312204411,4.11534177299659,337.696660306638));
#39217=CARTESIAN_POINT('Ctrl Pts',(125.275374900804,4.18900814700185,337.58073928102));
#39218=CARTESIAN_POINT('Ctrl Pts',(125.267627757498,4.25768322933087,337.461974122767));
#39219=CARTESIAN_POINT('Ctrl Pts',(125.25987887247,4.32637375127644,337.343182263585));
#39220=CARTESIAN_POINT('Ctrl Pts',(125.252129987442,4.3900705529706,337.221545337701));
#39221=CARTESIAN_POINT('Ctrl Pts',(125.244381102414,4.44854643423001,337.097526563598));
#39222=CARTESIAN_POINT('Ctrl Pts',(125.236623992639,4.50708438239397,336.973376154687));
#39223=CARTESIAN_POINT('Ctrl Pts',(125.228866882865,4.5603901734167,336.846839201508));
#39224=CARTESIAN_POINT('Ctrl Pts',(125.22110977309,4.6082843701736,336.71839990285));
#39225=CARTESIAN_POINT('Ctrl Pts',(125.213348518164,4.65620416005789,336.589891970337));
#39226=CARTESIAN_POINT('Ctrl Pts',(125.205587263238,4.69870647248079,336.459480038218));
#39227=CARTESIAN_POINT('Ctrl Pts',(125.197826008311,4.73566193697881,336.327663014906));
#39228=CARTESIAN_POINT('Ctrl Pts',(125.190052337907,4.77267651817627,336.195635127316));
#39229=CARTESIAN_POINT('Ctrl Pts',(125.182278667502,4.8041264305537,336.062198037635));
#39230=CARTESIAN_POINT('Ctrl Pts',(125.174504997097,4.82993338957599,335.927861258357));
#39231=CARTESIAN_POINT('Ctrl Pts',(125.16709319292,4.85453902844704,335.799777888472));
#39232=CARTESIAN_POINT('Ctrl Pts',(125.159681388743,4.87401520704816,335.670876989667));
#39233=CARTESIAN_POINT('Ctrl Pts',(125.152269584566,4.88833817252304,335.541602228166));
#39234=CARTESIAN_POINT('Ctrl Pts',(125.144494505788,4.90336314920172,335.405991325514));
#39235=CARTESIAN_POINT('Ctrl Pts',(125.136719427009,4.91276447311226,335.26954042976));
#39236=CARTESIAN_POINT('Ctrl Pts',(125.128944348231,4.91645797603193,335.132755536276));
#39237=CARTESIAN_POINT('Ctrl Pts',(125.121178837182,4.92014693386112,334.996138965312));
#39238=CARTESIAN_POINT('Ctrl Pts',(125.113413326133,4.91814203567155,334.859189601398));
#39239=CARTESIAN_POINT('Ctrl Pts',(125.105647815084,4.91041063744346,334.722420400277));
#39240=CARTESIAN_POINT('Ctrl Pts',(125.097890003562,4.90268690491922,334.585786806218));
#39241=CARTESIAN_POINT('Ctrl Pts',(125.09013219204,4.88924799350033,334.4493334072));
#39242=CARTESIAN_POINT('Ctrl Pts',(125.082374380517,4.87011327488168,334.313574656411));
#39243=CARTESIAN_POINT('Ctrl Pts',(125.074622406994,4.8509929557456,334.177918068387));
#39244=CARTESIAN_POINT('Ctrl Pts',(125.066870433471,4.82618541536519,334.042955473583));
#39245=CARTESIAN_POINT('Ctrl Pts',(125.059118459948,4.79576194309461,333.90919733789));
#39246=CARTESIAN_POINT('Ctrl Pts',(125.051369769391,4.76535135518257,333.775495848848));
#39247=CARTESIAN_POINT('Ctrl Pts',(125.043621078833,4.72932965226221,333.642998184732));
#39248=CARTESIAN_POINT('Ctrl Pts',(125.035872388276,4.68781939042985,333.512205516474));
#39249=CARTESIAN_POINT('Ctrl Pts',(125.028125309898,4.64631776515417,333.381440060723));
#39250=CARTESIAN_POINT('Ctrl Pts',(125.02037823152,4.59932997053408,333.252379267558));
#39251=CARTESIAN_POINT('Ctrl Pts',(125.012631153142,4.54702858153806,333.125509631613));
#39252=CARTESIAN_POINT('Ctrl Pts',(125.004884009836,4.49472675420606,332.998638932379));
#39253=CARTESIAN_POINT('Ctrl Pts',(124.997136866531,4.43711139264739,332.873959788366));
#39254=CARTESIAN_POINT('Ctrl Pts',(124.989389723225,4.37440326495255,332.751938804642));
#39255=CARTESIAN_POINT('Ctrl Pts',(124.981640838197,4.31168103913931,332.629890388012));
#39256=CARTESIAN_POINT('Ctrl Pts',(124.973891953169,4.24386394747163,332.510501668434));
#39257=CARTESIAN_POINT('Ctrl Pts',(124.966143068141,4.17121856919917,332.394214377492));
#39258=CARTESIAN_POINT('Ctrl Pts',(124.958385958366,4.09849608437156,332.277803658018));
#39259=CARTESIAN_POINT('Ctrl Pts',(124.950628848591,4.02093528310379,332.164501275064));
#39260=CARTESIAN_POINT('Ctrl Pts',(124.942871738816,3.93884623476317,332.054720148884));
#39261=CARTESIAN_POINT('Ctrl Pts',(124.93511048389,3.85671332065985,331.94488035918));
#39262=CARTESIAN_POINT('Ctrl Pts',(124.927349228964,3.77004758475939,331.838565878412));
#39263=CARTESIAN_POINT('Ctrl Pts',(124.919587974038,3.67919856000733,331.736155484932));
#39264=CARTESIAN_POINT('Ctrl Pts',(124.911814303633,3.58820420642329,331.633581268198));
#39265=CARTESIAN_POINT('Ctrl Pts',(124.904040633229,3.49301346313851,331.53492390008));
#39266=CARTESIAN_POINT('Ctrl Pts',(124.896266962824,3.39401242582346,331.440524938161));
#39267=CARTESIAN_POINT('Ctrl Pts',(124.888855158647,3.29961991061364,331.350520270629));
#39268=CARTESIAN_POINT('Ctrl Pts',(124.88144335447,3.20176407261195,331.264386663862));
#39269=CARTESIAN_POINT('Ctrl Pts',(124.874031550293,3.10080514617983,331.182384185395));
#39270=CARTESIAN_POINT('Ctrl Pts',(124.866256471514,2.99489792202207,331.096362521185));
#39271=CARTESIAN_POINT('Ctrl Pts',(124.858481392736,2.88524104854596,331.014615338097));
#39272=CARTESIAN_POINT('Ctrl Pts',(124.850706313957,2.77221447980072,330.937487238114));
#39273=CARTESIAN_POINT('Ctrl Pts',(124.842940802908,2.65932699744387,330.860454049169));
#39274=CARTESIAN_POINT('Ctrl Pts',(124.835175291859,2.54307839019052,330.788028851863));
#39275=CARTESIAN_POINT('Ctrl Pts',(124.82740978081,2.42388234791601,330.720516687033));
#39276=CARTESIAN_POINT('Ctrl Pts',(124.819651969288,2.30480448886452,330.653071460712));
#39277=CARTESIAN_POINT('Ctrl Pts',(124.811894157766,2.18278534843191,330.590529764128));
#39278=CARTESIAN_POINT('Ctrl Pts',(124.804136346244,2.0582680244126,330.533153707348));
#39279=CARTESIAN_POINT('Ctrl Pts',(124.796384372721,1.93384440362837,330.47582082787));
#39280=CARTESIAN_POINT('Ctrl Pts',(124.788632399198,1.80692669480055,330.423646013621));
#39281=CARTESIAN_POINT('Ctrl Pts',(124.780880425675,1.6779827383479,330.376845558246));
#39282=CARTESIAN_POINT('Ctrl Pts',(124.773131735117,1.54909338973727,330.330064922892));
#39283=CARTESIAN_POINT('Ctrl Pts',(124.765383044559,1.41817986689333,330.2886542526));
#39284=CARTESIAN_POINT('Ctrl Pts',(124.757634354002,1.28572993728018,330.252781699681));
#39285=CARTESIAN_POINT('Ctrl Pts',(124.749887275624,1.15330756498117,330.216916610347));
#39286=CARTESIAN_POINT('Ctrl Pts',(124.742140197246,1.0193497987886,330.186587448595));
#39287=CARTESIAN_POINT('Ctrl Pts',(124.734393118868,0.884359132638813,330.161912362615));
#39288=CARTESIAN_POINT('Ctrl Pts',(124.726645975562,0.749367335137269,330.137237069834));
#39289=CARTESIAN_POINT('Ctrl Pts',(124.718898832256,0.613343004915525,330.118216017625));
#39290=CARTESIAN_POINT('Ctrl Pts',(124.711151688951,0.476797990411733,330.104916064168));
#39291=CARTESIAN_POINT('Ctrl Pts',(124.703402803923,0.340222277689887,330.091613120599));
#39292=CARTESIAN_POINT('Ctrl Pts',(124.695653918894,0.203126036705078,330.08403387311));
#39293=CARTESIAN_POINT('Ctrl Pts',(124.687905033866,0.0660249902972504,
330.082193195828));
#39294=CARTESIAN_POINT('Ctrl Pts',(124.680147924092,-0.0712215765778929,
330.080350564833));
#39295=CARTESIAN_POINT('Ctrl Pts',(124.672390814317,-0.208472567608445,
330.0842586766));
#39296=CARTESIAN_POINT('Ctrl Pts',(124.664633704542,-0.345212953016926,
330.093880242027));
#39297=CARTESIAN_POINT('Ctrl Pts',(124.656872449616,-0.482026408115212,
330.103506948911));
#39298=CARTESIAN_POINT('Ctrl Pts',(124.64911119469,-0.618328325687482,330.118853149295));
#39299=CARTESIAN_POINT('Ctrl Pts',(124.641349939764,-0.75361103060421,330.139829892169));
#39300=CARTESIAN_POINT('Ctrl Pts',(124.633576269359,-0.889110143760274,
330.160840190995));
#39301=CARTESIAN_POINT('Ctrl Pts',(124.625802598954,-1.02358640260804,330.187498954982));
#39302=CARTESIAN_POINT('Ctrl Pts',(124.61802892855,-1.15654364556947,330.219666344449));
#39303=CARTESIAN_POINT('Ctrl Pts',(124.610617124372,-1.28331169688312,330.250336334197));
#39304=CARTESIAN_POINT('Ctrl Pts',(124.603205320195,-1.40869869330304,330.286013559068));
#39305=CARTESIAN_POINT('Ctrl Pts',(124.595793516018,-1.53229099500652,330.32653582777));
#39306=CARTESIAN_POINT('Ctrl Pts',(124.58801843724,-1.66194092357931,330.369044213569));
#39307=CARTESIAN_POINT('Ctrl Pts',(124.580243358461,-1.79002550018592,330.417018926481));
#39308=CARTESIAN_POINT('Ctrl Pts',(124.572468279683,-1.91604932672805,330.470326938945));
#39309=CARTESIAN_POINT('Ctrl Pts',(124.564702768634,-2.0419180729286,330.523569352506));
#39310=CARTESIAN_POINT('Ctrl Pts',(124.556937257585,-2.16573075819596,330.582131856382));
#39311=CARTESIAN_POINT('Ctrl Pts',(124.549171746536,-2.28700699585225,330.64583164503));
#39312=CARTESIAN_POINT('Ctrl Pts',(124.541413935014,-2.40816298776578,330.709468275152));
#39313=CARTESIAN_POINT('Ctrl Pts',(124.533656123492,-2.52678719303667,330.778231872843));
#39314=CARTESIAN_POINT('Ctrl Pts',(124.525898311969,-2.6424194120768,330.851891670511));
#39315=CARTESIAN_POINT('Ctrl Pts',(124.518146338446,-2.75796461420512,330.925496036844));
#39316=CARTESIAN_POINT('Ctrl Pts',(124.510394364923,-2.87052198339134,331.003989060088));
#39317=CARTESIAN_POINT('Ctrl Pts',(124.5026423914,-2.97965645839908,331.087094372155));
#39318=CARTESIAN_POINT('Ctrl Pts',(124.494893700843,-3.08874471489186,331.170164489073));
#39319=CARTESIAN_POINT('Ctrl Pts',(124.487145010285,-3.19441265002579,331.257842773511));
#39320=CARTESIAN_POINT('Ctrl Pts',(124.479396319727,-3.29625490197135,331.349810048267));
#39321=CARTESIAN_POINT('Ctrl Pts',(124.47164924135,-3.39807596478578,331.441758188464));
#39322=CARTESIAN_POINT('Ctrl Pts',(124.463902162972,-3.49607263772918,331.537993282208));
#39323=CARTESIAN_POINT('Ctrl Pts',(124.456155084594,-3.5898736391659,331.638156708393));
#39324=CARTESIAN_POINT('Ctrl Pts',(124.448407941288,-3.6836754267453,331.738320974044));
#39325=CARTESIAN_POINT('Ctrl Pts',(124.440660797982,-3.77328120550124,331.842413352502));
#39326=CARTESIAN_POINT('Ctrl Pts',(124.432913654677,-3.85835776240475,331.950039600291));
#39327=CARTESIAN_POINT('Ctrl Pts',(124.425164769648,-3.94345344632432,332.057690044746));
#39328=CARTESIAN_POINT('Ctrl Pts',(124.41741588462,-4.02401763981144,332.168875632897));
#39329=CARTESIAN_POINT('Ctrl Pts',(124.409666999592,-4.09975874767403,332.283170731649));
#39330=CARTESIAN_POINT('Ctrl Pts',(124.401909889818,-4.17558024793119,332.397587144399));
#39331=CARTESIAN_POINT('Ctrl Pts',(124.394152780043,-4.24656822007687,332.515119334403));
#39332=CARTESIAN_POINT('Ctrl Pts',(124.386395670268,-4.31247530914839,332.635314022859));
#39333=CARTESIAN_POINT('Ctrl Pts',(124.378634415342,-4.37841761686099,332.755572939514));
#39334=CARTESIAN_POINT('Ctrl Pts',(124.370873160416,-4.43927345816176,332.878496839467));
#39335=CARTESIAN_POINT('Ctrl Pts',(124.363111905489,-4.49484290171026,333.003610671376));
#39336=CARTESIAN_POINT('Ctrl Pts',(124.355338235085,-4.55050123825842,333.128924644641));
#39337=CARTESIAN_POINT('Ctrl Pts',(124.34756456468,-4.60085613479065,333.256435186504));
#39338=CARTESIAN_POINT('Ctrl Pts',(124.339790894275,-4.64575668397817,333.385649388834));
#39339=CARTESIAN_POINT('Ctrl Pts',(124.332379090098,-4.68856710179801,333.508848638956));
#39340=CARTESIAN_POINT('Ctrl Pts',(124.324967285921,-4.72641946073029,333.633596232795));
#39341=CARTESIAN_POINT('Ctrl Pts',(124.317555481744,-4.75922630665098,333.759456560784));
#39342=CARTESIAN_POINT('Ctrl Pts',(124.307455587595,-4.80393143690577,333.930963519126));
#39343=CARTESIAN_POINT('Ctrl Pts',(124.297355693447,-4.83938417614909,334.104974579676));
#39344=CARTESIAN_POINT('Ctrl Pts',(124.287255799298,-4.86535496713038,334.280622417419));
#39345=CARTESIAN_POINT('Ctrl Pts',(124.277360004687,-4.8908009381128,334.452720748408));
#39346=CARTESIAN_POINT('Ctrl Pts',(124.267464210076,-4.90714435346763,334.626390601291));
#39347=CARTESIAN_POINT('Ctrl Pts',(124.257568415465,-4.91421409236322,334.800794284924));
#39348=CARTESIAN_POINT('Ctrl Pts',(124.253891026484,-4.91684128714015,334.865604662434));
#39349=CARTESIAN_POINT('Ctrl Pts',(124.250213637502,-4.91818828344244,334.930516140544));
#39350=CARTESIAN_POINT('Ctrl Pts',(124.246536248521,-4.91824792744739,334.995484841147));
#39351=CARTESIAN_POINT('',(127.746536248441,-4.91824840624245,335.003959418342));
#39352=CARTESIAN_POINT('Ctrl Pts',(127.746536248441,-4.91824840624245,335.003959418342));
#39353=CARTESIAN_POINT('Ctrl Pts',(127.737429000281,-4.9181185842084,335.165219724011));
#39354=CARTESIAN_POINT('Ctrl Pts',(127.728321752122,-4.91005377499314,335.326144681731));
#39355=CARTESIAN_POINT('Ctrl Pts',(127.719214503963,-4.89417593406791,335.486029823046));
#39356=CARTESIAN_POINT('Ctrl Pts',(127.71004726698,-4.87819350688481,335.646968116909));
#39357=CARTESIAN_POINT('Ctrl Pts',(127.700880029996,-4.85429488696353,335.806852778631));
#39358=CARTESIAN_POINT('Ctrl Pts',(127.691712793013,-4.82265339123684,335.964985663361));
#39359=CARTESIAN_POINT('Ctrl Pts',(127.682478322858,-4.79077983451745,336.124278305977));
#39360=CARTESIAN_POINT('Ctrl Pts',(127.673243852703,-4.75104948174692,336.28179331331));
#39361=CARTESIAN_POINT('Ctrl Pts',(127.664009382549,-4.70368766144363,336.4368386987));
#39362=CARTESIAN_POINT('Ctrl Pts',(127.661476886043,-4.69069897422996,336.479358939727));
#39363=CARTESIAN_POINT('Ctrl Pts',(127.658944389537,-4.67713660103905,336.52169356915));
#39364=CARTESIAN_POINT('Ctrl Pts',(127.656411893031,-4.6630058067537,336.563828605916));
#39365=CARTESIAN_POINT('Ctrl Pts',(127.648636814253,-4.61962251342256,336.693188401455));
#39366=CARTESIAN_POINT('Ctrl Pts',(127.640861735474,-4.5707835927889,336.820945951818));
#39367=CARTESIAN_POINT('Ctrl Pts',(127.633086656696,-4.51662541614281,336.946606768907));
#39368=CARTESIAN_POINT('Ctrl Pts',(127.625321145647,-4.46253388458095,337.07211295236));
#39369=CARTESIAN_POINT('Ctrl Pts',(127.617555634598,-4.40313627426551,337.195527180802));
#39370=CARTESIAN_POINT('Ctrl Pts',(127.609790123549,-4.33861863191982,337.316370313499));
#39371=CARTESIAN_POINT('Ctrl Pts',(127.602032312027,-4.27416495900428,337.437093629878));
#39372=CARTESIAN_POINT('Ctrl Pts',(127.594274500505,-4.20460153953952,337.555250581073));
#39373=CARTESIAN_POINT('Ctrl Pts',(127.586516688982,-4.13016224482694,337.670382536998));
#39374=CARTESIAN_POINT('Ctrl Pts',(127.578764715459,-4.05577896804424,337.785427852476));
#39375=CARTESIAN_POINT('Ctrl Pts',(127.571012741937,-3.97652733085012,337.897452376836));
#39376=CARTESIAN_POINT('Ctrl Pts',(127.563260768414,-3.89268663417267,338.006022925833));
#39377=CARTESIAN_POINT('Ctrl Pts',(127.555512077856,-3.80888144408013,338.114547495138));
#39378=CARTESIAN_POINT('Ctrl Pts',(127.547763387298,-3.72049129833228,338.219620689684));
#39379=CARTESIAN_POINT('Ctrl Pts',(127.540014696741,-3.62783810535521,338.320839313161));
#39380=CARTESIAN_POINT('Ctrl Pts',(127.532267618363,-3.53520418964882,338.422036877257));
#39381=CARTESIAN_POINT('Ctrl Pts',(127.524520539985,-3.43830925470008,338.519381177332));
#39382=CARTESIAN_POINT('Ctrl Pts',(127.516773461607,-3.33751442170336,338.612503362963));
#39383=CARTESIAN_POINT('Ctrl Pts',(127.509026318302,-3.23671874394886,338.705626329048));
#39384=CARTESIAN_POINT('Ctrl Pts',(127.501279174996,-3.13202339005494,338.794526844864));
#39385=CARTESIAN_POINT('Ctrl Pts',(127.49353203169,-3.02382484559053,338.878874368382));
#39386=CARTESIAN_POINT('Ctrl Pts',(127.485783146662,-2.91560197579636,338.963240855013));
#39387=CARTESIAN_POINT('Ctrl Pts',(127.478034261634,-2.80387465642282,339.043052072208));
#39388=CARTESIAN_POINT('Ctrl Pts',(127.470285376606,-2.68907048078475,339.118019306884));
#39389=CARTESIAN_POINT('Ctrl Pts',(127.462528266831,-2.57414445080831,339.193066112558));
#39390=CARTESIAN_POINT('Ctrl Pts',(127.454771157056,-2.45613536860487,339.263258451128));
#39391=CARTESIAN_POINT('Ctrl Pts',(127.447014047282,-2.33549817369035,339.328352035497));
#39392=CARTESIAN_POINT('Ctrl Pts',(127.439252792356,-2.21479651411619,339.393480403796));
#39393=CARTESIAN_POINT('Ctrl Pts',(127.431491537429,-2.09146429476056,339.453504417898));
#39394=CARTESIAN_POINT('Ctrl Pts',(127.423730282503,-1.96597790680437,339.508227360333));
#39395=CARTESIAN_POINT('Ctrl Pts',(127.415956612099,-1.84029078152338,339.563037841643));
#39396=CARTESIAN_POINT('Ctrl Pts',(127.408182941694,-1.71244296628371,339.612530164576));
#39397=CARTESIAN_POINT('Ctrl Pts',(127.400409271289,-1.58292837745497,339.656556755195));
#39398=CARTESIAN_POINT('Ctrl Pts',(127.392997467112,-1.45944272389427,339.698533897428));
#39399=CARTESIAN_POINT('Ctrl Pts',(127.385585662935,-1.3344422571681,339.735542633752));
#39400=CARTESIAN_POINT('Ctrl Pts',(127.378173858758,-1.20836316771759,339.767498454893));
#39401=CARTESIAN_POINT('Ctrl Pts',(127.370398779979,-1.07610456652419,339.801020526018));
#39402=CARTESIAN_POINT('Ctrl Pts',(127.362623701201,-0.942240974504719,
339.829087776953));
#39403=CARTESIAN_POINT('Ctrl Pts',(127.354848622423,-0.807262015579741,
339.85154728934));
#39404=CARTESIAN_POINT('Ctrl Pts',(127.347083111374,-0.672449156856947,
339.873979163867));
#39405=CARTESIAN_POINT('Ctrl Pts',(127.339317600325,-0.536524044056986,
339.890816966678));
#39406=CARTESIAN_POINT('Ctrl Pts',(127.331552089276,-0.399990277402321,
339.901957857885));
#39407=CARTESIAN_POINT('Ctrl Pts',(127.323794277753,-0.263591884374801,
339.913087702867));
#39408=CARTESIAN_POINT('Ctrl Pts',(127.316036466231,-0.12658642552593,339.918531845505));
#39409=CARTESIAN_POINT('Ctrl Pts',(127.308278654709,0.0105138661390176,
339.91823876211));
#39410=CARTESIAN_POINT('Ctrl Pts',(127.300526681186,0.147510985486694,339.917945899269));
#39411=CARTESIAN_POINT('Ctrl Pts',(127.292774707663,0.284602406302951,339.91192440489));
#39412=CARTESIAN_POINT('Ctrl Pts',(127.28502273414,0.421272708956044,339.900174728231));
#39413=CARTESIAN_POINT('Ctrl Pts',(127.277274043582,0.557885131654915,339.888430027566));
#39414=CARTESIAN_POINT('Ctrl Pts',(127.269525353025,0.694076402276577,339.870962002953));
#39415=CARTESIAN_POINT('Ctrl Pts',(127.261776662467,0.829333261321776,339.847823161396));
#39416=CARTESIAN_POINT('Ctrl Pts',(127.254029584089,0.964561979047763,339.824689134068));
#39417=CARTESIAN_POINT('Ctrl Pts',(127.246282505712,1.09885628686149,339.795886702492));
#39418=CARTESIAN_POINT('Ctrl Pts',(127.238535427334,1.23171058717457,339.761519935057));
#39419=CARTESIAN_POINT('Ctrl Pts',(127.230788284028,1.36456600093455,339.727152879595));
#39420=CARTESIAN_POINT('Ctrl Pts',(127.223041140722,1.49598100470378,339.687221493146));
#39421=CARTESIAN_POINT('Ctrl Pts',(127.215293997416,1.625463077546,339.641880313627));
#39422=CARTESIAN_POINT('Ctrl Pts',(127.207545112388,1.75497426070709,339.596528940447));
#39423=CARTESIAN_POINT('Ctrl Pts',(127.19979622736,1.88255127936962,339.545765483179));
#39424=CARTESIAN_POINT('Ctrl Pts',(127.192047342332,2.00771995326452,339.489793274947));
#39425=CARTESIAN_POINT('Ctrl Pts',(127.184290232557,2.13302148248321,339.433761657236));
#39426=CARTESIAN_POINT('Ctrl Pts',(127.176533122783,2.25590920321444,339.372510404433));
#39427=CARTESIAN_POINT('Ctrl Pts',(127.168776013008,2.37593149535021,339.306289887119));
#39428=CARTESIAN_POINT('Ctrl Pts',(127.161014758082,2.49601792356133,339.240033983678));
#39429=CARTESIAN_POINT('Ctrl Pts',(127.153253503156,2.6132355382701,339.168803727451));
#39430=CARTESIAN_POINT('Ctrl Pts',(127.145492248229,2.72716111295764,339.092893270838));
#39431=CARTESIAN_POINT('Ctrl Pts',(127.137718577825,2.84126893143643,339.016861382233));
#39432=CARTESIAN_POINT('Ctrl Pts',(127.12994490742,2.95207387039609,338.936134562693));
#39433=CARTESIAN_POINT('Ctrl Pts',(127.122171237015,3.0591845452739,338.851048296303));
#39434=CARTESIAN_POINT('Ctrl Pts',(127.114759432838,3.16130919246735,338.769922816083));
#39435=CARTESIAN_POINT('Ctrl Pts',(127.107347628661,3.26007555345974,338.684834807632));
#39436=CARTESIAN_POINT('Ctrl Pts',(127.099935824484,3.35517651492205,338.596105339978));
#39437=CARTESIAN_POINT('Ctrl Pts',(127.092160745706,3.45493865779627,338.503026976803));
#39438=CARTESIAN_POINT('Ctrl Pts',(127.084385666927,3.55098227862865,338.405647026398));
#39439=CARTESIAN_POINT('Ctrl Pts',(127.076610588149,3.6429138215132,338.304294471068));
#39440=CARTESIAN_POINT('Ctrl Pts',(127.0688450771,3.73473223678157,338.203066636509));
#39441=CARTESIAN_POINT('Ctrl Pts',(127.061079566051,3.8224483823009,338.097876210574));
#39442=CARTESIAN_POINT('Ctrl Pts',(127.053314055002,3.90570325084063,337.98909102887));
#39443=CARTESIAN_POINT('Ctrl Pts',(127.045556243479,3.98887557193586,337.880413707991));
#39444=CARTESIAN_POINT('Ctrl Pts',(127.037798431957,4.0675951827806,337.768149032728));
#39445=CARTESIAN_POINT('Ctrl Pts',(127.030040620435,4.14154155733407,337.652699868318));
#39446=CARTESIAN_POINT('Ctrl Pts',(127.022288646912,4.21543228489564,337.537337583066));
#39447=CARTESIAN_POINT('Ctrl Pts',(127.014536673389,4.28455671591711,337.418795906462));
#39448=CARTESIAN_POINT('Ctrl Pts',(127.006784699866,4.34863630505158,337.297508508991));
#39449=CARTESIAN_POINT('Ctrl Pts',(126.999036009308,4.41268875644203,337.176272476805));
#39450=CARTESIAN_POINT('Ctrl Pts',(126.991287318751,4.47170043306779,337.052293381393));
#39451=CARTESIAN_POINT('Ctrl Pts',(126.983538628193,4.52543773502323,336.92603124817));
#39452=CARTESIAN_POINT('Ctrl Pts',(126.975791549815,4.57916385648417,336.799795384839));
#39453=CARTESIAN_POINT('Ctrl Pts',(126.968044471437,4.62761763306284,336.671277787946));
#39454=CARTESIAN_POINT('Ctrl Pts',(126.96029739306,4.67061297022109,336.540959942666));
#39455=CARTESIAN_POINT('Ctrl Pts',(126.952550249754,4.71360866772167,336.410641005198));
#39456=CARTESIAN_POINT('Ctrl Pts',(126.944803106448,4.75114571208938,336.278522160442));
#39457=CARTESIAN_POINT('Ctrl Pts',(126.937055963142,4.7830875262143,336.145101209096));
#39458=CARTESIAN_POINT('Ctrl Pts',(126.929307078114,4.81503652153716,336.011650261887));
#39459=CARTESIAN_POINT('Ctrl Pts',(126.921558193086,4.84138769249563,335.876897005623));
#39460=CARTESIAN_POINT('Ctrl Pts',(126.913809308058,4.86205542010043,335.741350223829));
#39461=CARTESIAN_POINT('Ctrl Pts',(126.906052198283,4.88274508464486,335.605659571281));
#39462=CARTESIAN_POINT('Ctrl Pts',(126.898295088508,4.89773919640854,335.469174097736));
#39463=CARTESIAN_POINT('Ctrl Pts',(126.890537978734,4.90700389979862,335.332409070064));
#39464=CARTESIAN_POINT('Ctrl Pts',(126.882776723808,4.91627355394997,335.195570959535));
#39465=CARTESIAN_POINT('Ctrl Pts',(126.875015468881,4.91980768912263,335.058453387763));
#39466=CARTESIAN_POINT('Ctrl Pts',(126.867254213955,4.91762463218933,334.921571437698));
#39467=CARTESIAN_POINT('Ctrl Pts',(126.859480543551,4.9154380830764,334.784470521123));
#39468=CARTESIAN_POINT('Ctrl Pts',(126.851706873146,4.90751608875082,334.647606369875));
#39469=CARTESIAN_POINT('Ctrl Pts',(126.843933202741,4.89392896429312,334.511489657271));
#39470=CARTESIAN_POINT('Ctrl Pts',(126.836521398564,4.88097432374781,334.381709210387));
#39471=CARTESIAN_POINT('Ctrl Pts',(126.829109594387,4.86287014731348,334.25260846662));
#39472=CARTESIAN_POINT('Ctrl Pts',(126.82169779021,4.83972023214225,334.124619432993));
#39473=CARTESIAN_POINT('Ctrl Pts',(126.813922711432,4.81543567066841,333.990357275569));
#39474=CARTESIAN_POINT('Ctrl Pts',(126.806147632653,4.78552150707733,333.856894266986));
#39475=CARTESIAN_POINT('Ctrl Pts',(126.798372553875,4.75004141392361,333.724739388003));
#39476=CARTESIAN_POINT('Ctrl Pts',(126.790607042826,4.7146049812833,333.592747134012));
#39477=CARTESIAN_POINT('Ctrl Pts',(126.782841531777,4.67361634746703,333.462060180604));
#39478=CARTESIAN_POINT('Ctrl Pts',(126.775076020728,4.62719055387269,333.333179481572));
#39479=CARTESIAN_POINT('Ctrl Pts',(126.767318209205,4.58081079158786,333.204426568129));
#39480=CARTESIAN_POINT('Ctrl Pts',(126.759560397683,4.52900472945568,333.07747671043));
#39481=CARTESIAN_POINT('Ctrl Pts',(126.751802586161,4.47193769041654,332.952817459157));
#39482=CARTESIAN_POINT('Ctrl Pts',(126.744050612638,4.414913596134,332.828252017924));
#39483=CARTESIAN_POINT('Ctrl Pts',(126.736298639115,4.35263656728711,332.705974106043));
#39484=CARTESIAN_POINT('Ctrl Pts',(126.728546665592,4.28532054976733,332.586452642221));
#39485=CARTESIAN_POINT('Ctrl Pts',(126.720797975034,4.21803304062094,332.46698179581));
#39486=CARTESIAN_POINT('Ctrl Pts',(126.713049284477,4.14571097862224,332.35026541553));
#39487=CARTESIAN_POINT('Ctrl Pts',(126.705300593919,4.06861479464466,332.236748886674));
#39488=CARTESIAN_POINT('Ctrl Pts',(126.697553515541,3.99153465117209,332.12325597588));
#39489=CARTESIAN_POINT('Ctrl Pts',(126.689806437164,3.90968258092601,332.012961915422));
#39490=CARTESIAN_POINT('Ctrl Pts',(126.682059358786,3.82336276862943,331.906283755423));
#39491=CARTESIAN_POINT('Ctrl Pts',(126.67431221548,3.73704223288972,331.799604701359));
#39492=CARTESIAN_POINT('Ctrl Pts',(126.666565072174,3.64625412628549,331.696541912057));
#39493=CARTESIAN_POINT('Ctrl Pts',(126.658817928868,3.55134315033103,331.597479626645));
#39494=CARTESIAN_POINT('Ctrl Pts',(126.65106904384,3.45641083637419,331.498395069927));
#39495=CARTESIAN_POINT('Ctrl Pts',(126.643320158812,3.35735407898259,331.403313088986));
#39496=CARTESIAN_POINT('Ctrl Pts',(126.635571273784,3.25455439172946,331.312581014615));
#39497=CARTESIAN_POINT('Ctrl Pts',(126.627814164009,3.15164559182608,331.221752636283));
#39498=CARTESIAN_POINT('Ctrl Pts',(126.620057054235,3.04498621956935,331.135283646546));
#39499=CARTESIAN_POINT('Ctrl Pts',(126.61229994446,2.93499125265941,331.053481355763));
#39500=CARTESIAN_POINT('Ctrl Pts',(126.604538689534,2.82493750795619,330.971635352451));
#39501=CARTESIAN_POINT('Ctrl Pts',(126.596777434607,2.71154493990857,330.894461236896));
#39502=CARTESIAN_POINT('Ctrl Pts',(126.589016179681,2.59525661048028,330.82222233858));
#39503=CARTESIAN_POINT('Ctrl Pts',(126.581242509277,2.47878225762314,330.749867881569));
#39504=CARTESIAN_POINT('Ctrl Pts',(126.573468838872,2.35940322727646,330.682464610102));
#39505=CARTESIAN_POINT('Ctrl Pts',(126.565695168467,2.23758700705245,330.620229749362));
#39506=CARTESIAN_POINT('Ctrl Pts',(126.55828336429,2.1214413611875,330.560891936363));
#39507=CARTESIAN_POINT('Ctrl Pts',(126.550871560113,2.00308058282386,330.50625230431));
#39508=CARTESIAN_POINT('Ctrl Pts',(126.543459755936,1.88292412648035,330.456457351755));
#39509=CARTESIAN_POINT('Ctrl Pts',(126.535684677158,1.75687844428347,330.404221800244));
#39510=CARTESIAN_POINT('Ctrl Pts',(126.527909598379,1.62845828266413,330.357152766548));
#39511=CARTESIAN_POINT('Ctrl Pts',(126.520134519601,1.49812611127402,330.315472145753));
#39512=CARTESIAN_POINT('Ctrl Pts',(126.512369008552,1.36795432191816,330.273842815615));
#39513=CARTESIAN_POINT('Ctrl Pts',(126.504603497503,1.23587557302824,330.23758882294));
#39514=CARTESIAN_POINT('Ctrl Pts',(126.496837986454,1.10237338283778,330.206884521805));
#39515=CARTESIAN_POINT('Ctrl Pts',(126.489080174932,0.969003560457524,330.176210664074));
#39516=CARTESIAN_POINT('Ctrl Pts',(126.481322363409,0.83421348391091,330.151075634573));
#39517=CARTESIAN_POINT('Ctrl Pts',(126.473564551887,0.698502610697266,330.131604251363));
#39518=CARTESIAN_POINT('Ctrl Pts',(126.465812578364,0.562893864219401,330.112147520986));
#39519=CARTESIAN_POINT('Ctrl Pts',(126.458060604841,0.426366085669455,330.098346008742));
#39520=CARTESIAN_POINT('Ctrl Pts',(126.450308631318,0.289429377190495,330.090273561784));
#39521=CARTESIAN_POINT('Ctrl Pts',(126.442559940761,0.152550661488875,330.082204533512));
#39522=CARTESIAN_POINT('Ctrl Pts',(126.434811250203,0.015263749689991,330.079859767816));
#39523=CARTESIAN_POINT('Ctrl Pts',(126.427062559645,-0.121915890122222,
330.083261286357));
#39524=CARTESIAN_POINT('Ctrl Pts',(126.419315481267,-0.259066988564671,
330.086662097183));
#39525=CARTESIAN_POINT('Ctrl Pts',(126.41156840289,-0.396110468905335,330.095806804505));
#39526=CARTESIAN_POINT('Ctrl Pts',(126.403821324512,-0.532531012990603,
330.110665302651));
#39527=CARTESIAN_POINT('Ctrl Pts',(126.396074181206,-0.668952700411195,
330.125523925325));
#39528=CARTESIAN_POINT('Ctrl Pts',(126.3883270379,-0.804751052586834,330.146096392015));
#39529=CARTESIAN_POINT('Ctrl Pts',(126.380579894594,-0.939416416870888,
330.172300769703));
#39530=CARTESIAN_POINT('Ctrl Pts',(126.372831009566,-1.07411205678781,330.198511038691));
#39531=CARTESIAN_POINT('Ctrl Pts',(126.365082124538,-1.20767381834649,330.230355663574));
#39532=CARTESIAN_POINT('Ctrl Pts',(126.35733323951,-1.33960316478618,330.267701782073));
#39533=CARTESIAN_POINT('Ctrl Pts',(126.349576129735,-1.47167254239741,330.305087540128));
#39534=CARTESIAN_POINT('Ctrl Pts',(126.341819019961,-1.60210566704428,330.3479863498));
#39535=CARTESIAN_POINT('Ctrl Pts',(126.334061910186,-1.73041954664402,330.396215550757));
#39536=CARTESIAN_POINT('Ctrl Pts',(126.32630065526,-1.8588019930783,330.444470523857));
#39537=CARTESIAN_POINT('Ctrl Pts',(126.318539400334,-1.98506257832049,330.498061411276));
#39538=CARTESIAN_POINT('Ctrl Pts',(126.310778145408,-2.10874009674039,330.556758135449));
#39539=CARTESIAN_POINT('Ctrl Pts',(126.303004475003,-2.23261545888335,330.615548755251));
#39540=CARTESIAN_POINT('Ctrl Pts',(126.295230804598,-2.35389915113358,330.67946135092));
#39541=CARTESIAN_POINT('Ctrl Pts',(126.287457134194,-2.47215551982878,330.74822035516));
#39542=CARTESIAN_POINT('Ctrl Pts',(126.280045330016,-2.58490702611154,330.81377861121));
#39543=CARTESIAN_POINT('Ctrl Pts',(126.272633525839,-2.69490646710385,330.883742074728));
#39544=CARTESIAN_POINT('Ctrl Pts',(126.265221721662,-2.801803658141,330.957837296233));
#39545=CARTESIAN_POINT('Ctrl Pts',(126.257489796435,-2.91331781424917,331.03513274261));
#39546=CARTESIAN_POINT('Ctrl Pts',(126.249757871209,-3.02181683019522,331.117175227558));
#39547=CARTESIAN_POINT('Ctrl Pts',(126.242025945982,-3.12686658200773,331.203700691354));
#39548=CARTESIAN_POINT('Ctrl Pts',(126.234303559797,-3.23178673168168,331.290119406825));
#39549=CARTESIAN_POINT('Ctrl Pts',(126.226581173613,-3.33326578005632,331.38100984988));
#39550=CARTESIAN_POINT('Ctrl Pts',(126.218858787429,-3.43089795556801,331.476064376158));
#39551=CARTESIAN_POINT('Ctrl Pts',(126.211144028533,-3.52843370120097,331.571025018465));
#39552=CARTESIAN_POINT('Ctrl Pts',(126.203429269637,-3.62212985195588,331.670141286756));
#39553=CARTESIAN_POINT('Ctrl Pts',(126.195714510741,-3.71161349914195,331.773065185739));
#39554=CARTESIAN_POINT('Ctrl Pts',(126.188005474514,-3.80103076898046,331.87591273764));
#39555=CARTESIAN_POINT('Ctrl Pts',(126.180296438286,-3.88624149514754,331.982562001969));
#39556=CARTESIAN_POINT('Ctrl Pts',(126.172587402058,-3.966909764782,332.092628338073));
#39557=CARTESIAN_POINT('Ctrl Pts',(126.164881483907,-4.04754540649268,332.202650155607));
#39558=CARTESIAN_POINT('Ctrl Pts',(126.157175565757,-4.1236420114915,332.31608597817));
#39559=CARTESIAN_POINT('Ctrl Pts',(126.149469647606,-4.19490428962288,332.432518536892));
#39560=CARTESIAN_POINT('Ctrl Pts',(126.141765161666,-4.26615332304912,332.548929455625));
#39561=CARTESIAN_POINT('Ctrl Pts',(126.134060675726,-4.33256961003524,332.668335665489));
#39562=CARTESIAN_POINT('Ctrl Pts',(126.126356189786,-4.39390176642594,332.79029179992));
#39563=CARTESIAN_POINT('Ctrl Pts',(126.118651420408,-4.45523617914033,332.912252420947));
#39564=CARTESIAN_POINT('Ctrl Pts',(126.110946651031,-4.51148591145028,333.036762799581));
#39565=CARTESIAN_POINT('Ctrl Pts',(126.103241881654,-4.56244624654336,333.163354331968));
#39566=CARTESIAN_POINT('Ctrl Pts',(126.095535113322,-4.61341980298235,333.28997870775));
#39567=CARTESIAN_POINT('Ctrl Pts',(126.087828344989,-4.65910108471449,333.418684944373));
#39568=CARTESIAN_POINT('Ctrl Pts',(126.080121576657,-4.69933425155995,333.548986335483));
#39569=CARTESIAN_POINT('Ctrl Pts',(126.072406696856,-4.73960976431207,333.679424870421));
#39570=CARTESIAN_POINT('Ctrl Pts',(126.064691817054,-4.77442559528901,333.811461533829));
#39571=CARTESIAN_POINT('Ctrl Pts',(126.056976937253,-4.80367624537959,333.944596005278));
#39572=CARTESIAN_POINT('Ctrl Pts',(126.049257603452,-4.8329437826263,334.077807338697));
#39573=CARTESIAN_POINT('Ctrl Pts',(126.041538269651,-4.85663967119378,334.212117353458));
#39574=CARTESIAN_POINT('Ctrl Pts',(126.03381893585,-4.87471008483557,334.347018643986));
#39575=CARTESIAN_POINT('Ctrl Pts',(126.026088189024,-4.89280721556078,334.482119385898));
#39576=CARTESIAN_POINT('Ctrl Pts',(126.018357442198,-4.90526222560895,334.617812756118));
#39577=CARTESIAN_POINT('Ctrl Pts',(126.010626695372,-4.91207334932376,334.753588812423));
#39578=CARTESIAN_POINT('Ctrl Pts',(126.005929879758,-4.91621144787085,334.836079562092));
#39579=CARTESIAN_POINT('Ctrl Pts',(126.001233064145,-4.91826730934574,334.918600853459));
#39580=CARTESIAN_POINT('Ctrl Pts',(125.996536248531,-4.91824989020686,335.001039220942));
#39581=CARTESIAN_POINT('',(129.496536248543,-4.91824916909057,334.997141112125));
#39582=CARTESIAN_POINT('Ctrl Pts',(129.49653624849,-4.91824916909112,334.997141113067));
#39583=CARTESIAN_POINT('Ctrl Pts',(129.488710570362,-4.9183298433808,335.13592808418));
#39584=CARTESIAN_POINT('Ctrl Pts',(129.480884892233,-4.91253157919313,335.274726350522));
#39585=CARTESIAN_POINT('Ctrl Pts',(129.473059214105,-4.90087810992756,335.413009460101));
#39586=CARTESIAN_POINT('Ctrl Pts',(129.465232246285,-4.88922272014096,335.551315359084));
#39587=CARTESIAN_POINT('Ctrl Pts',(129.457405278465,-4.87171023496562,335.689105553739));
#39588=CARTESIAN_POINT('Ctrl Pts',(129.449578310645,-4.84841629440405,335.825858643266));
#39589=CARTESIAN_POINT('Ctrl Pts',(129.441748490757,-4.82511386576545,335.96266156424));
#39590=CARTESIAN_POINT('Ctrl Pts',(129.433918670869,-4.79602584993982,336.098426253253));
#39591=CARTESIAN_POINT('Ctrl Pts',(129.426088850981,-4.76127898355548,336.232641676747));
#39592=CARTESIAN_POINT('Ctrl Pts',(129.418254615085,-4.72651251998405,336.366932797563));
#39593=CARTESIAN_POINT('Ctrl Pts',(129.410420379188,-4.68608094482974,336.499672545629));
#39594=CARTESIAN_POINT('Ctrl Pts',(129.402586143292,-4.64016072426206,336.630365454589));
#39595=CARTESIAN_POINT('Ctrl Pts',(129.394741224013,-4.59417788325398,336.761236586723));
#39596=CARTESIAN_POINT('Ctrl Pts',(129.386896304734,-4.54269157665094,336.890054947805));
#39597=CARTESIAN_POINT('Ctrl Pts',(129.379051385455,-4.48592650900079,337.016344816331));
#39598=CARTESIAN_POINT('Ctrl Pts',(129.371200172618,-4.42911590178636,337.142736000434));
#39599=CARTESIAN_POINT('Ctrl Pts',(129.363348959782,-4.36701826387414,337.266594311415));
#39600=CARTESIAN_POINT('Ctrl Pts',(129.355497746946,-4.29990366529128,337.387469692313));
#39601=CARTESIAN_POINT('Ctrl Pts',(129.347634273421,-4.23268425855185,337.508533835807));
#39602=CARTESIAN_POINT('Ctrl Pts',(129.339770799897,-4.16043244475512,337.626605425462));
#39603=CARTESIAN_POINT('Ctrl Pts',(129.331907326373,-4.08346121829752,337.741263858362));
#39604=CARTESIAN_POINT('Ctrl Pts',(129.32988491714,-4.06366496432108,337.770752896833));
#39605=CARTESIAN_POINT('Ctrl Pts',(129.327862507908,-4.04355673962888,337.80001634081));
#39606=CARTESIAN_POINT('Ctrl Pts',(129.325840098675,-4.02314228273049,337.829047407769));
#39607=CARTESIAN_POINT('Ctrl Pts',(129.318065019897,-3.94465964526313,337.940656289398));
#39608=CARTESIAN_POINT('Ctrl Pts',(129.310289941118,-3.86140513775162,338.049173195096));
#39609=CARTESIAN_POINT('Ctrl Pts',(129.30251486234,-3.77365052583071,338.154163085732));
#39610=CARTESIAN_POINT('Ctrl Pts',(129.294749351291,-3.68600390154654,338.259023779624));
#39611=CARTESIAN_POINT('Ctrl Pts',(129.286983840242,-3.59386843949686,338.360365797199));
#39612=CARTESIAN_POINT('Ctrl Pts',(129.279218329193,-3.49755913856428,338.457782979706));
#39613=CARTESIAN_POINT('Ctrl Pts',(129.271460517671,-3.40134532858401,338.555103572794));
#39614=CARTESIAN_POINT('Ctrl Pts',(129.263702706148,-3.30096618835245,338.648506798915));
#39615=CARTESIAN_POINT('Ctrl Pts',(129.255944894626,-3.19677670314018,338.737619800456));
#39616=CARTESIAN_POINT('Ctrl Pts',(129.248192921103,-3.09266562381965,338.826665741638));
#39617=CARTESIAN_POINT('Ctrl Pts',(129.24044094758,-2.98475020279728,338.911427631432));
#39618=CARTESIAN_POINT('Ctrl Pts',(129.232688974057,-2.87342170844965,338.991569960293));
#39619=CARTESIAN_POINT('Ctrl Pts',(129.2249402835,-2.76214036178536,339.071678348829));
#39620=CARTESIAN_POINT('Ctrl Pts',(129.217191592942,-2.64744913323816,339.14717083966));
#39621=CARTESIAN_POINT('Ctrl Pts',(129.209442902384,-2.52977157371988,339.217752819607));
#39622=CARTESIAN_POINT('Ctrl Pts',(129.201695824007,-2.41211849800069,339.288320114383));
#39623=CARTESIAN_POINT('Ctrl Pts',(129.193948745629,-2.29148066217425,339.35397872953));
#39624=CARTESIAN_POINT('Ctrl Pts',(129.186201667251,-2.16830940283761,339.41447815671));
#39625=CARTESIAN_POINT('Ctrl Pts',(129.178454523945,-2.04513711120714,339.474978090933));
#39626=CARTESIAN_POINT('Ctrl Pts',(129.170707380639,-1.919431704554,339.530318578621));
#39627=CARTESIAN_POINT('Ctrl Pts',(129.162960237334,-1.79166748630491,339.580295916316));
#39628=CARTESIAN_POINT('Ctrl Pts',(129.155211352306,-1.66387454394753,339.630284489976));
#39629=CARTESIAN_POINT('Ctrl Pts',(129.147462467278,-1.53402223288998,339.674907371972));
#39630=CARTESIAN_POINT('Ctrl Pts',(129.139713582249,-1.40260273933468,339.714009823718));
#39631=CARTESIAN_POINT('Ctrl Pts',(129.131956472475,-1.2710437557708,339.753153779211));
#39632=CARTESIAN_POINT('Ctrl Pts',(129.1241993627,-1.13791464209848,339.786765488022));
#39633=CARTESIAN_POINT('Ctrl Pts',(129.116442252925,-1.00372112120168,339.81474059253));
#39634=CARTESIAN_POINT('Ctrl Pts',(129.108680997999,-0.869455891578076,
339.842730646039));
#39635=CARTESIAN_POINT('Ctrl Pts',(129.100919743073,-0.734125506830217,
339.865078029869));
#39636=CARTESIAN_POINT('Ctrl Pts',(129.093158488147,-0.598242680140097,
339.881730098864));
#39637=CARTESIAN_POINT('Ctrl Pts',(129.085384817742,-0.462142485211244,
339.898408805743));
#39638=CARTESIAN_POINT('Ctrl Pts',(129.077611147338,-0.325488472218683,
339.909373960736));
#39639=CARTESIAN_POINT('Ctrl Pts',(129.069837476933,-0.188796132337487,
339.914625019563));
#39640=CARTESIAN_POINT('Ctrl Pts',(129.062425672756,-0.0584668537638033,
339.919631640338));
#39641=CARTESIAN_POINT('Ctrl Pts',(129.055013868579,0.0718969759700748,
339.919444175783));
#39642=CARTESIAN_POINT('Ctrl Pts',(129.047602064402,0.201853183231733,339.914106058575));
#39643=CARTESIAN_POINT('Ctrl Pts',(129.039826985623,0.338178931330607,339.90850630434));
#39644=CARTESIAN_POINT('Ctrl Pts',(129.032051906845,0.474486903596368,339.897220537189));
#39645=CARTESIAN_POINT('Ctrl Pts',(129.024276828066,0.610264198362322,339.880241866004));
#39646=CARTESIAN_POINT('Ctrl Pts',(129.016511317017,0.745874410522877,339.863284088155));
#39647=CARTESIAN_POINT('Ctrl Pts',(129.008745805968,0.880954860385049,339.840647393207));
#39648=CARTESIAN_POINT('Ctrl Pts',(129.000980294919,1.01499353642109,339.812376874635));
#39649=CARTESIAN_POINT('Ctrl Pts',(128.993222483397,1.14889931271969,339.784134386365));
#39650=CARTESIAN_POINT('Ctrl Pts',(128.985464671875,1.28176499076853,339.75026927098));
#39651=CARTESIAN_POINT('Ctrl Pts',(128.977706860353,1.41308492374687,339.710878268516));
#39652=CARTESIAN_POINT('Ctrl Pts',(128.96995488683,1.5443060343113,339.671516909032));
#39653=CARTESIAN_POINT('Ctrl Pts',(128.962202913307,1.67398334225606,339.626638051423));
#39654=CARTESIAN_POINT('Ctrl Pts',(128.954450939784,1.80162297267577,339.576389158149));
#39655=CARTESIAN_POINT('Ctrl Pts',(128.946702249226,1.92920854763621,339.526161545312));
#39656=CARTESIAN_POINT('Ctrl Pts',(128.938953558668,2.05475779848533,339.470568562943));
#39657=CARTESIAN_POINT('Ctrl Pts',(128.931204868111,2.1777937710154,339.409806951945));
#39658=CARTESIAN_POINT('Ctrl Pts',(128.923457789733,2.30080414488376,339.349057982909));
#39659=CARTESIAN_POINT('Ctrl Pts',(128.915710711355,2.42130193028902,339.283142697214));
#39660=CARTESIAN_POINT('Ctrl Pts',(128.907963632977,2.53883222529564,339.212305068997));
#39661=CARTESIAN_POINT('Ctrl Pts',(128.900216489671,2.65636350531941,339.141466847093));
#39662=CARTESIAN_POINT('Ctrl Pts',(128.892469346366,2.77092691056876,339.065706402156));
#39663=CARTESIAN_POINT('Ctrl Pts',(128.88472220306,2.88209446965961,338.985312350426));
#39664=CARTESIAN_POINT('Ctrl Pts',(128.876973318032,2.99328702157801,338.904900224406));
#39665=CARTESIAN_POINT('Ctrl Pts',(128.869224433003,3.10108189147329,338.819852647668));
#39666=CARTESIAN_POINT('Ctrl Pts',(128.861475547975,3.20508260617299,338.730499772163));
#39667=CARTESIAN_POINT('Ctrl Pts',(128.853718438201,3.30919370830552,338.641052056593));
#39668=CARTESIAN_POINT('Ctrl Pts',(128.845961328426,3.40950231367455,338.547290168998));
#39669=CARTESIAN_POINT('Ctrl Pts',(128.838204218651,3.50564699005738,338.449582908643));
#39670=CARTESIAN_POINT('Ctrl Pts',(128.830442963725,3.60184304308115,338.351823436652));
#39671=CARTESIAN_POINT('Ctrl Pts',(128.822681708799,3.6938704713474,338.250114680653));
#39672=CARTESIAN_POINT('Ctrl Pts',(128.814920453873,3.78140754589906,338.144859302786));
#39673=CARTESIAN_POINT('Ctrl Pts',(128.807146783468,3.86908465124167,338.039435550616));
#39674=CARTESIAN_POINT('Ctrl Pts',(128.799373113063,3.952256811642,337.930454150252));
#39675=CARTESIAN_POINT('Ctrl Pts',(128.791599442659,4.03064460755032,337.81834829468));
#39676=CARTESIAN_POINT('Ctrl Pts',(128.784187638482,4.10538343270009,337.711460993656));
#39677=CARTESIAN_POINT('Ctrl Pts',(128.776775834304,4.17577313830021,337.601733820215));
#39678=CARTESIAN_POINT('Ctrl Pts',(128.769364030127,4.24161096229037,337.489562111512));
#39679=CARTESIAN_POINT('Ctrl Pts',(128.761588951349,4.31067569415507,337.371892533224));
#39680=CARTESIAN_POINT('Ctrl Pts',(128.75381387257,4.3749493169291,337.25116087516));
#39681=CARTESIAN_POINT('Ctrl Pts',(128.746038793792,4.4341484752029,337.127794718096));
#39682=CARTESIAN_POINT('Ctrl Pts',(128.738273282743,4.49327478514374,337.004580370941));
#39683=CARTESIAN_POINT('Ctrl Pts',(128.730507771694,4.54733888776425,336.878738324307));
#39684=CARTESIAN_POINT('Ctrl Pts',(128.722742260645,4.59610162431328,336.750723542278));
#39685=CARTESIAN_POINT('Ctrl Pts',(128.714984449123,4.644816012467,336.622835687277));
#39686=CARTESIAN_POINT('Ctrl Pts',(128.707226637601,4.68823935668187,336.492779746926));
#39687=CARTESIAN_POINT('Ctrl Pts',(128.699468826078,4.7261793732111,336.361033282008));
#39688=CARTESIAN_POINT('Ctrl Pts',(128.691716852555,4.76409083867489,336.229385960483));
#39689=CARTESIAN_POINT('Ctrl Pts',(128.683964879032,4.79652708207503,336.096051020687));
#39690=CARTESIAN_POINT('Ctrl Pts',(128.676212905509,4.82334484368842,335.961523572963));
#39691=CARTESIAN_POINT('Ctrl Pts',(128.668464214952,4.85015124796372,335.827053097694));
#39692=CARTESIAN_POINT('Ctrl Pts',(128.660715524394,4.87134382671436,335.691391501495));
#39693=CARTESIAN_POINT('Ctrl Pts',(128.652966833837,4.88682991627327,335.555046333126));
#39694=CARTESIAN_POINT('Ctrl Pts',(128.645219755459,4.90231278382191,335.418729532508));
#39695=CARTESIAN_POINT('Ctrl Pts',(128.637472677081,4.91209147968396,335.281729830745));
#39696=CARTESIAN_POINT('Ctrl Pts',(128.629725598703,4.91612499337729,335.144561792985));
#39697=CARTESIAN_POINT('Ctrl Pts',(128.621978455397,4.92015854087534,335.007392605625));
#39698=CARTESIAN_POINT('Ctrl Pts',(128.614231312092,4.91844679867661,334.870055470159));
#39699=CARTESIAN_POINT('Ctrl Pts',(128.606484168786,4.91100087046202,334.733066463663));
#39700=CARTESIAN_POINT('Ctrl Pts',(128.598735283758,4.90355326824466,334.59604665913));
#39701=CARTESIAN_POINT('Ctrl Pts',(128.59098639873,4.89036893592378,334.45937552953));
#39702=CARTESIAN_POINT('Ctrl Pts',(128.583237513701,4.87151095093534,334.323565141779));
#39703=CARTESIAN_POINT('Ctrl Pts',(128.575480403927,4.85263294988685,334.187610603479));
#39704=CARTESIAN_POINT('Ctrl Pts',(128.567723294152,4.82806932035802,334.0525190198));
#39705=CARTESIAN_POINT('Ctrl Pts',(128.559966184377,4.79793460180347,333.918793905253));
#39706=CARTESIAN_POINT('Ctrl Pts',(128.552204929451,4.76778378021887,333.784997332281));
#39707=CARTESIAN_POINT('Ctrl Pts',(128.544443674525,4.73205603940615,333.652569060615));
#39708=CARTESIAN_POINT('Ctrl Pts',(128.536682419599,4.69091588054836,333.521997542587));
#39709=CARTESIAN_POINT('Ctrl Pts',(128.528908749194,4.64970991084394,333.391217152683));
#39710=CARTESIAN_POINT('Ctrl Pts',(128.52113507879,4.60307435467188,333.262299819513));
#39711=CARTESIAN_POINT('Ctrl Pts',(128.513361408385,4.5512222833044,333.135714938521));
#39712=CARTESIAN_POINT('Ctrl Pts',(128.505949604208,4.50178393833409,333.015022614194));
#39713=CARTESIAN_POINT('Ctrl Pts',(128.498537800031,4.44760392592213,332.896450739364));
#39714=CARTESIAN_POINT('Ctrl Pts',(128.491125995854,4.38890496733028,332.780383760592));
#39715=CARTESIAN_POINT('Ctrl Pts',(128.483350917075,4.32732899792243,332.658627993444));
#39716=CARTESIAN_POINT('Ctrl Pts',(128.475575838297,4.26058531626217,332.539244105077));
#39717=CARTESIAN_POINT('Ctrl Pts',(128.467800759519,4.18888014427416,332.422701763589));
#39718=CARTESIAN_POINT('Ctrl Pts',(128.46003524847,4.11726321006525,332.306302834873));
#39719=CARTESIAN_POINT('Ctrl Pts',(128.452269737421,4.04069713645387,332.192738825323));
#39720=CARTESIAN_POINT('Ctrl Pts',(128.444504226372,3.95943508992144,332.082457055809));
#39721=CARTESIAN_POINT('Ctrl Pts',(128.436746414849,3.87825361494438,331.97228463099));
#39722=CARTESIAN_POINT('Ctrl Pts',(128.428988603327,3.79238566326635,331.86538828251));
#39723=CARTESIAN_POINT('Ctrl Pts',(128.421230791805,3.70212877017079,331.762188141418));
#39724=CARTESIAN_POINT('Ctrl Pts',(128.413478818282,3.61193979825039,331.659065661706));
#39725=CARTESIAN_POINT('Ctrl Pts',(128.405726844759,3.51736871529613,331.559634145954));
#39726=CARTESIAN_POINT('Ctrl Pts',(128.397974871236,3.41875434410055,331.464281996936));
#39727=CARTESIAN_POINT('Ctrl Pts',(128.390226180678,3.32018173614913,331.368970229608));
#39728=CARTESIAN_POINT('Ctrl Pts',(128.382477490121,3.21756952608372,331.277734664049));
#39729=CARTESIAN_POINT('Ctrl Pts',(128.374728799563,3.11129437685753,331.190927886869));
#39730=CARTESIAN_POINT('Ctrl Pts',(128.366981721185,3.00504133906383,331.104139170564));
#39731=CARTESIAN_POINT('Ctrl Pts',(128.359234642807,2.89512718052339,331.021777656929));
#39732=CARTESIAN_POINT('Ctrl Pts',(128.35148756443,2.78196241692162,330.944156293281));
#39733=CARTESIAN_POINT('Ctrl Pts',(128.343740421124,2.66879670489037,330.866534279091));
#39734=CARTESIAN_POINT('Ctrl Pts',(128.335993277818,2.55238065579436,330.79365271522));
#39735=CARTESIAN_POINT('Ctrl Pts',(128.328246134512,2.43315425869544,330.725781543265));
#39736=CARTESIAN_POINT('Ctrl Pts',(128.320497249484,2.31390105697087,330.65789511243));
#39737=CARTESIAN_POINT('Ctrl Pts',(128.312748364456,2.19183658960441,330.59502150834));
#39738=CARTESIAN_POINT('Ctrl Pts',(128.304999479428,2.06742559940844,330.537384796623));
#39739=CARTESIAN_POINT('Ctrl Pts',(128.297242369653,1.94288255810227,330.479686908705));
#39740=CARTESIAN_POINT('Ctrl Pts',(128.289485259878,1.81598837393559,330.427237181336));
#39741=CARTESIAN_POINT('Ctrl Pts',(128.281728150104,1.68722844687343,330.380211776438));
#39742=CARTESIAN_POINT('Ctrl Pts',(128.273966895177,1.55839971462311,330.333161242667));
#39743=CARTESIAN_POINT('Ctrl Pts',(128.266205640251,1.42770362513454,330.291540925603));
#39744=CARTESIAN_POINT('Ctrl Pts',(128.258444385325,1.29563994942319,330.255476822276));
#39745=CARTESIAN_POINT('Ctrl Pts',(128.25067071492,1.16336501487029,330.219355028137));
#39746=CARTESIAN_POINT('Ctrl Pts',(128.242897044516,1.02971850368519,330.188807295995));
#39747=CARTESIAN_POINT('Ctrl Pts',(128.235123374111,0.895210445600456,330.16390846648));
#39748=CARTESIAN_POINT('Ctrl Pts',(128.227711569934,0.766963769981202,330.140168683468));
#39749=CARTESIAN_POINT('Ctrl Pts',(128.220299765757,0.637934237252592,330.121563766662));
#39750=CARTESIAN_POINT('Ctrl Pts',(128.21288796158,0.508565663983887,330.108114471094));
#39751=CARTESIAN_POINT('Ctrl Pts',(128.205112882802,0.372856351569223,330.094005985487));
#39752=CARTESIAN_POINT('Ctrl Pts',(128.197337804023,0.236345056999165,330.085526699067));
#39753=CARTESIAN_POINT('Ctrl Pts',(128.189562725245,0.0995383327161246,
330.082757359778));
#39754=CARTESIAN_POINT('Ctrl Pts',(128.181797214196,-0.0371000421829576,
330.079991428337));
#39755=CARTESIAN_POINT('Ctrl Pts',(128.174031703147,-0.174032736386184,
330.082921471233));
#39756=CARTESIAN_POINT('Ctrl Pts',(128.166266192098,-0.310746585322844,
330.091576666361));
#39757=CARTESIAN_POINT('Ctrl Pts',(128.158508380576,-0.447324882079973,
330.100223279838));
#39758=CARTESIAN_POINT('Ctrl Pts',(128.150750569053,-0.583684377803953,
330.114583724443));
#39759=CARTESIAN_POINT('Ctrl Pts',(128.142992757531,-0.719310761919096,
330.134635153425));
#39760=CARTESIAN_POINT('Ctrl Pts',(128.135240784008,-0.854835082879417,
330.154671493071));
#39761=CARTESIAN_POINT('Ctrl Pts',(128.127488810485,-0.989627005227994,
330.180390235761));
#39762=CARTESIAN_POINT('Ctrl Pts',(128.119736836962,-1.12317655633233,330.211716645205));
#39763=CARTESIAN_POINT('Ctrl Pts',(128.111988146404,-1.25666954912299,330.243029787897));
#39764=CARTESIAN_POINT('Ctrl Pts',(128.104239455847,-1.38892083738134,330.279945784856));
#39765=CARTESIAN_POINT('Ctrl Pts',(128.096490765289,-1.51943008956658,330.322338697018));
#39766=CARTESIAN_POINT('Ctrl Pts',(128.088743686911,-1.64991218821143,330.364722788979));
#39767=CARTESIAN_POINT('Ctrl Pts',(128.080996608534,-1.77865260019195,330.412581408881));
#39768=CARTESIAN_POINT('Ctrl Pts',(128.073249530156,-1.90516600784046,330.465738699075));
#39769=CARTESIAN_POINT('Ctrl Pts',(128.06550238685,-2.03168047579345,330.518896434778));
#39770=CARTESIAN_POINT('Ctrl Pts',(128.057755243544,-2.15596754182973,330.577352777937));
#39771=CARTESIAN_POINT('Ctrl Pts',(128.050008100238,-2.27756210297438,330.640883813249));
#39772=CARTESIAN_POINT('Ctrl Pts',(128.04225921521,-2.39918400115769,330.704429131687));
#39773=CARTESIAN_POINT('Ctrl Pts',(128.034510330182,-2.51811184353597,330.773051231566));
#39774=CARTESIAN_POINT('Ctrl Pts',(128.026761445154,-2.6339057095397,330.84648055551));
#39775=CARTESIAN_POINT('Ctrl Pts',(128.019004335379,-2.74982248034938,330.919987818097));
#39776=CARTESIAN_POINT('Ctrl Pts',(128.011247225604,-2.86259829929943,330.998312287688));
#39777=CARTESIAN_POINT('Ctrl Pts',(128.00349011583,-2.97182235029787,331.081141112419));
#39778=CARTESIAN_POINT('Ctrl Pts',(127.995728860904,-3.0811047671369,331.164014198227));
#39779=CARTESIAN_POINT('Ctrl Pts',(127.987967605977,-3.18683133304892,331.25139618642));
#39780=CARTESIAN_POINT('Ctrl Pts',(127.980206351051,-3.28862563967027,331.342934993112));
#39781=CARTESIAN_POINT('Ctrl Pts',(127.972432680646,-3.39058278400735,331.434620232063));
#39782=CARTESIAN_POINT('Ctrl Pts',(127.964659010242,-3.48859481951027,331.530475303851));
#39783=CARTESIAN_POINT('Ctrl Pts',(127.956885339837,-3.58232280474365,331.630111814153));
#39784=CARTESIAN_POINT('Ctrl Pts',(127.94947353566,-3.67168772971594,331.72511022093));
#39785=CARTESIAN_POINT('Ctrl Pts',(127.942061731483,-3.75715828505088,331.823545719694));
#39786=CARTESIAN_POINT('Ctrl Pts',(127.934649927306,-3.83847684278656,331.925056327363));
#39787=CARTESIAN_POINT('Ctrl Pts',(127.926811857355,-3.92447217247712,332.032404986963));
#39788=CARTESIAN_POINT('Ctrl Pts',(127.918973787404,-4.00610492627406,332.14354388457));
#39789=CARTESIAN_POINT('Ctrl Pts',(127.911135717454,-4.08302188865518,332.258081817548));
#39790=CARTESIAN_POINT('Ctrl Pts',(127.903388132755,-4.1590508963803,332.371297487038));
#39791=CARTESIAN_POINT('Ctrl Pts',(127.895640548056,-4.23047215722734,332.487833817112));
#39792=CARTESIAN_POINT('Ctrl Pts',(127.887892963357,-4.29698302741908,332.607277716789));
#39793=CARTESIAN_POINT('Ctrl Pts',(127.880152880545,-4.36342949598585,332.726605960467));
#39794=CARTESIAN_POINT('Ctrl Pts',(127.872412797734,-4.42497484252336,332.848835833053));
#39795=CARTESIAN_POINT('Ctrl Pts',(127.864672714922,-4.48135934721705,332.973524867261));
#39796=CARTESIAN_POINT('Ctrl Pts',(127.85693843481,-4.53770158073825,333.098120422742));
#39797=CARTESIAN_POINT('Ctrl Pts',(127.849204154699,-4.58889050980646,333.225171115613));
#39798=CARTESIAN_POINT('Ctrl Pts',(127.841469874587,-4.63471225796807,333.354209810352));
#39799=CARTESIAN_POINT('Ctrl Pts',(127.833558739079,-4.6815817860558,333.486199159736));
#39800=CARTESIAN_POINT('Ctrl Pts',(127.825647603571,-4.7228355025048,333.620268161879));
#39801=CARTESIAN_POINT('Ctrl Pts',(127.817736468063,-4.75829647276027,333.755894803557));
#39802=CARTESIAN_POINT('Ctrl Pts',(127.810007972526,-4.79293877538075,333.88839030863));
#39803=CARTESIAN_POINT('Ctrl Pts',(127.80227947699,-4.82205279167517,334.022371915563));
#39804=CARTESIAN_POINT('Ctrl Pts',(127.794550981453,-4.84552409401785,334.157337958139));
#39805=CARTESIAN_POINT('Ctrl Pts',(127.786548525959,-4.86982740783749,334.297088281315));
#39806=CARTESIAN_POINT('Ctrl Pts',(127.778546070465,-4.88808046340052,334.43789369095));
#39807=CARTESIAN_POINT('Ctrl Pts',(127.770543614972,-4.90021423700222,334.579187103357));
#39808=CARTESIAN_POINT('Ctrl Pts',(127.762541159478,-4.91234801060392,334.720480515765));
#39809=CARTESIAN_POINT('Ctrl Pts',(127.754538703984,-4.91836247964961,334.862261464752));
#39810=CARTESIAN_POINT('Ctrl Pts',(127.74653624849,-4.91824840624315,335.00395941747));
#39811=CARTESIAN_POINT('',(131.246536248453,-4.91824924060785,334.99726691378));
#39812=CARTESIAN_POINT('Ctrl Pts',(131.246536248453,-4.91824924060785,334.99726691378));
#39813=CARTESIAN_POINT('Ctrl Pts',(131.238860999982,-4.91832419279384,335.132145034037));
#39814=CARTESIAN_POINT('Ctrl Pts',(131.231185751512,-4.91284661490259,335.267247101451));
#39815=CARTESIAN_POINT('Ctrl Pts',(131.223510503042,-4.90178762207131,335.402071101434));
#39816=CARTESIAN_POINT('Ctrl Pts',(131.215843894781,-4.8907410786093,335.536743326858));
#39817=CARTESIAN_POINT('Ctrl Pts',(131.208177286519,-4.87412564910301,335.671137710913));
#39818=CARTESIAN_POINT('Ctrl Pts',(131.200510678257,-4.85196444990179,335.804750917607));
#39819=CARTESIAN_POINT('Ctrl Pts',(131.192850758201,-4.82982258371629,335.938247562638));
#39820=CARTESIAN_POINT('Ctrl Pts',(131.185190838145,-4.80214463739249,336.070963992175));
#39821=CARTESIAN_POINT('Ctrl Pts',(131.177530918089,-4.76900560663304,336.202401175317));
#39822=CARTESIAN_POINT('Ctrl Pts',(131.169875333428,-4.73588533204745,336.333763967066));
#39823=CARTESIAN_POINT('Ctrl Pts',(131.162219748767,-4.69731021811577,336.463848564326));
#39824=CARTESIAN_POINT('Ctrl Pts',(131.154564164106,-4.65340641976804,336.592165743559));
#39825=CARTESIAN_POINT('Ctrl Pts',(131.146910803518,-4.60951537619533,336.720445644541));
#39826=CARTESIAN_POINT('Ctrl Pts',(131.139257442931,-4.56029885568008,336.846958768903));
#39827=CARTESIAN_POINT('Ctrl Pts',(131.131604082343,-4.50593285082086,336.971231139769));
#39828=CARTESIAN_POINT('Ctrl Pts',(131.123951191523,-4.45157018297827,337.095495882725));
#39829=CARTESIAN_POINT('Ctrl Pts',(131.116298300703,-4.39205882023487,337.217519777963));
#39830=CARTESIAN_POINT('Ctrl Pts',(131.108645409882,-4.32762265436903,337.336849422597));
#39831=CARTESIAN_POINT('Ctrl Pts',(131.100991235131,-4.26317567800085,337.456199087252));
#39832=CARTESIAN_POINT('Ctrl Pts',(131.09333706038,-4.19380244644444,337.572853249405));
#39833=CARTESIAN_POINT('Ctrl Pts',(131.085682885629,-4.11977222899054,337.686384157886));
#39834=CARTESIAN_POINT('Ctrl Pts',(131.078021004012,-4.04566747169431,337.800029378823));
#39835=CARTESIAN_POINT('Ctrl Pts',(131.070359122394,-3.96689658280152,337.910544728399));
#39836=CARTESIAN_POINT('Ctrl Pts',(131.062697240777,-3.88377171888825,338.017532153609));
#39837=CARTESIAN_POINT('Ctrl Pts',(131.055031479518,-3.80060476418162,338.124573752569));
#39838=CARTESIAN_POINT('Ctrl Pts',(131.047365718259,-3.71307970316364,338.228083563571));
#39839=CARTESIAN_POINT('Ctrl Pts',(131.039699957,-3.62154737670412,338.327698553173));
#39840=CARTESIAN_POINT('Ctrl Pts',(131.032022091977,-3.52987052633862,338.427470828708));
#39841=CARTESIAN_POINT('Ctrl Pts',(131.024344226953,-3.43417405392277,338.52333571341));
#39842=CARTESIAN_POINT('Ctrl Pts',(131.016666361929,-3.33484438255584,338.614968327197));
#39843=CARTESIAN_POINT('Ctrl Pts',(131.009533676059,-3.24256777425054,338.700094419875));
#39844=CARTESIAN_POINT('Ctrl Pts',(131.002400990189,-3.14715616375519,338.781568205919));
#39845=CARTESIAN_POINT('Ctrl Pts',(130.995268304319,-3.04894185816097,338.859162682248));
#39846=CARTESIAN_POINT('Ctrl Pts',(130.987493225541,-2.94188205248691,338.943745569709));
#39847=CARTESIAN_POINT('Ctrl Pts',(130.979718146762,-2.83113069276856,339.024003704274));
#39848=CARTESIAN_POINT('Ctrl Pts',(130.971943067984,-2.71707235433044,339.099597649018));
#39849=CARTESIAN_POINT('Ctrl Pts',(130.964177556935,-2.60315437193928,339.1750985706));
#39850=CARTESIAN_POINT('Ctrl Pts',(130.956412045886,-2.4859378305606,339.24594650861));
#39851=CARTESIAN_POINT('Ctrl Pts',(130.948646534837,-2.36584050375049,339.311842039467));
#39852=CARTESIAN_POINT('Ctrl Pts',(130.940888723315,-2.24586225378951,339.377672234713));
#39853=CARTESIAN_POINT('Ctrl Pts',(130.933130911793,-2.12300924308282,339.438559607818));
#39854=CARTESIAN_POINT('Ctrl Pts',(130.92537310027,-1.99772807037857,339.494248059389));
#39855=CARTESIAN_POINT('Ctrl Pts',(130.917621126747,-1.87254117572994,339.549894603634));
#39856=CARTESIAN_POINT('Ctrl Pts',(130.909869153224,-1.74493011191208,339.600349855562));
#39857=CARTESIAN_POINT('Ctrl Pts',(130.902117179701,-1.61536559900807,339.645403862318));
#39858=CARTESIAN_POINT('Ctrl Pts',(130.894368489144,-1.4858559567518,339.690438788676));
#39859=CARTESIAN_POINT('Ctrl Pts',(130.886619798586,-1.35439487924633,339.730076891286));
#39860=CARTESIAN_POINT('Ctrl Pts',(130.878871108028,-1.221472361358,339.764156623468));
#39861=CARTESIAN_POINT('Ctrl Pts',(130.871124029651,-1.08857749910972,339.798229265078));
#39862=CARTESIAN_POINT('Ctrl Pts',(130.863376951273,-0.954222179675249,
339.826745739536));
#39863=CARTESIAN_POINT('Ctrl Pts',(130.855629872895,-0.818910447437517,
339.849594698692));
#39864=CARTESIAN_POINT('Ctrl Pts',(130.847882729589,-0.683597581157139,
339.872443849343));
#39865=CARTESIAN_POINT('Ctrl Pts',(130.840135586283,-0.547328671503624,
339.889625324869));
#39866=CARTESIAN_POINT('Ctrl Pts',(130.832388442977,-0.410616423522549,
339.901079188835));
#39867=CARTESIAN_POINT('Ctrl Pts',(130.824639557949,-0.273873439725831,
339.912535627873));
#39868=CARTESIAN_POINT('Ctrl Pts',(130.816890672921,-0.136687308699211,
339.918261860369));
#39869=CARTESIAN_POINT('Ctrl Pts',(130.809141787893,0.000426092826129061,
339.918249981543));
#39870=CARTESIAN_POINT('Ctrl Pts',(130.801384678118,0.137685027932541,339.918238090108));
#39871=CARTESIAN_POINT('Ctrl Pts',(130.793627568344,0.274870687840066,339.912475921059));
#39872=CARTESIAN_POINT('Ctrl Pts',(130.785870458569,0.411468593600158,339.901007718723));
#39873=CARTESIAN_POINT('Ctrl Pts',(130.778109203643,0.548139492913627,339.889533388146));
#39874=CARTESIAN_POINT('Ctrl Pts',(130.770347948717,0.684221624655794,339.872346997582));
#39875=CARTESIAN_POINT('Ctrl Pts',(130.76258669379,0.819208561864751,339.84954434918));
#39876=CARTESIAN_POINT('Ctrl Pts',(130.754813023386,0.954411434181009,339.826705223973));
#39877=CARTESIAN_POINT('Ctrl Pts',(130.747039352981,1.08851522848843,339.798231969095));
#39878=CARTESIAN_POINT('Ctrl Pts',(130.739265682576,1.22102571788834,339.764271115161));
#39879=CARTESIAN_POINT('Ctrl Pts',(130.731853878399,1.34736781212674,339.731891147147));
#39880=CARTESIAN_POINT('Ctrl Pts',(130.724442074222,1.47226132420035,339.69452306066));
#39881=CARTESIAN_POINT('Ctrl Pts',(130.717030270045,1.5952948434285,339.652334620922));
#39882=CARTESIAN_POINT('Ctrl Pts',(130.709255191267,1.7243586019316,339.60807840008));
#39883=CARTESIAN_POINT('Ctrl Pts',(130.701480112488,1.85178329517504,339.558377500741));
#39884=CARTESIAN_POINT('Ctrl Pts',(130.69370503371,1.97707536763083,339.503371631701));
#39885=CARTESIAN_POINT('Ctrl Pts',(130.685939522661,2.10221326021498,339.448433450885));
#39886=CARTESIAN_POINT('Ctrl Pts',(130.678174011612,2.22522339918631,339.388203445045));
#39887=CARTESIAN_POINT('Ctrl Pts',(130.670408500563,2.3456279116231,339.322870893598));
#39888=CARTESIAN_POINT('Ctrl Pts',(130.662650689041,2.46591304263514,339.257603119565));
#39889=CARTESIAN_POINT('Ctrl Pts',(130.654892877518,2.58359734705257,339.187243053212));
#39890=CARTESIAN_POINT('Ctrl Pts',(130.647135065996,2.69822378522158,339.112027658876));
#39891=CARTESIAN_POINT('Ctrl Pts',(130.639383092473,2.81276396336065,339.03686886651));
#39892=CARTESIAN_POINT('Ctrl Pts',(130.63163111895,2.92425053007613,338.956862232423));
#39893=CARTESIAN_POINT('Ctrl Pts',(130.623879145427,3.03225219788486,338.872289977639));
#39894=CARTESIAN_POINT('Ctrl Pts',(130.61613045487,3.14020812692348,338.787753539254));
#39895=CARTESIAN_POINT('Ctrl Pts',(130.608381764312,3.24468178532352,338.698655566337));
#39896=CARTESIAN_POINT('Ctrl Pts',(130.600633073754,3.3452721606967,338.605320683846));
#39897=CARTESIAN_POINT('Ctrl Pts',(130.592885995377,3.44584160740214,338.512005220457));
#39898=CARTESIAN_POINT('Ctrl Pts',(130.585138916999,3.54252909179903,338.414454866604));
#39899=CARTESIAN_POINT('Ctrl Pts',(130.577391838621,3.63496821151331,338.313033227088));
#39900=CARTESIAN_POINT('Ctrl Pts',(130.569644695315,3.72740810595632,338.211610737561));
#39901=CARTESIAN_POINT('Ctrl Pts',(130.561897552009,3.81559930139824,338.106317186544));
#39902=CARTESIAN_POINT('Ctrl Pts',(130.554150408703,3.8992139418947,337.997551283604));
#39903=CARTESIAN_POINT('Ctrl Pts',(130.546401523675,3.98284738073777,337.888760927779));
#39904=CARTESIAN_POINT('Ctrl Pts',(130.538652638647,4.06190197904431,337.776496976435));
#39905=CARTESIAN_POINT('Ctrl Pts',(130.530903753619,4.13609191901683,337.661188963592));
#39906=CARTESIAN_POINT('Ctrl Pts',(130.523146643844,4.21036060495799,337.545758561633));
#39907=CARTESIAN_POINT('Ctrl Pts',(130.51538953407,4.27975410636193,337.427277973183));
#39908=CARTESIAN_POINT('Ctrl Pts',(130.507632424295,4.34403121514666,337.306203777712));
#39909=CARTESIAN_POINT('Ctrl Pts',(130.499871169369,4.40834267156309,337.185064884061));
#39910=CARTESIAN_POINT('Ctrl Pts',(130.492109914443,4.46753211895922,337.061329974206));
#39911=CARTESIAN_POINT('Ctrl Pts',(130.484348659517,4.52140606271786,336.935476757421));
#39912=CARTESIAN_POINT('Ctrl Pts',(130.476574989112,4.57536618722908,336.809422216505));
#39913=CARTESIAN_POINT('Ctrl Pts',(130.468801318707,4.62399367772629,336.681242962884));
#39914=CARTESIAN_POINT('Ctrl Pts',(130.461027648303,4.66714430039421,336.551433898623));
#39915=CARTESIAN_POINT('Ctrl Pts',(130.453615844125,4.70828625119613,336.427667477532));
#39916=CARTESIAN_POINT('Ctrl Pts',(130.446204039948,4.74444967582734,336.302419842963));
#39917=CARTESIAN_POINT('Ctrl Pts',(130.438792235771,4.77555301371775,336.176127746323));
#39918=CARTESIAN_POINT('Ctrl Pts',(130.431017156993,4.80818081884981,336.043645697824));
#39919=CARTESIAN_POINT('Ctrl Pts',(130.423242078214,4.83534308541445,335.909595546319));
#39920=CARTESIAN_POINT('Ctrl Pts',(130.415466999436,4.85689020630341,335.774467937628));
#39921=CARTESIAN_POINT('Ctrl Pts',(130.407701488387,4.87841081208837,335.639506612062));
#39922=CARTESIAN_POINT('Ctrl Pts',(130.399935977338,4.89432995974505,335.503470849738));
#39923=CARTESIAN_POINT('Ctrl Pts',(130.392170466289,4.90454821391293,335.366864934143));
#39924=CARTESIAN_POINT('Ctrl Pts',(130.384412654766,4.91475633665202,335.230394463711));
#39925=CARTESIAN_POINT('Ctrl Pts',(130.376654843244,4.9192747856339,335.093355352278));
#39926=CARTESIAN_POINT('Ctrl Pts',(130.368897031722,4.91805549884353,334.956260169241));
#39927=CARTESIAN_POINT('Ctrl Pts',(130.361145058199,4.91683712960514,334.819268154675));
#39928=CARTESIAN_POINT('Ctrl Pts',(130.353393084676,4.90988962248244,334.682220541777));
#39929=CARTESIAN_POINT('Ctrl Pts',(130.345641111153,4.89721690874973,334.545632735383));
#39930=CARTESIAN_POINT('Ctrl Pts',(130.337892420595,4.88454956191884,334.409102774006));
#39931=CARTESIAN_POINT('Ctrl Pts',(130.330143730038,4.86616186692838,334.273032620223));
#39932=CARTESIAN_POINT('Ctrl Pts',(130.32239503948,4.84210979701792,334.1379351671));
#39933=CARTESIAN_POINT('Ctrl Pts',(130.314647961102,4.81806273134149,334.00286582213));
#39934=CARTESIAN_POINT('Ctrl Pts',(130.306900882724,4.78835370337467,333.868769159856));
#39935=CARTESIAN_POINT('Ctrl Pts',(130.299153804347,4.75309019480281,333.736150063271));
#39936=CARTESIAN_POINT('Ctrl Pts',(130.291406661041,4.71782639068884,333.603529855211));
#39937=CARTESIAN_POINT('Ctrl Pts',(130.283659517735,4.67700811356214,333.472387615289));
#39938=CARTESIAN_POINT('Ctrl Pts',(130.275912374429,4.63079322514058,333.343214809189));
#39939=CARTESIAN_POINT('Ctrl Pts',(130.268163489401,4.58456794663097,333.214012962299));
#39940=CARTESIAN_POINT('Ctrl Pts',(130.260414604373,4.53294377419524,333.086781798251));
#39941=CARTESIAN_POINT('Ctrl Pts',(130.252665719345,4.47612723974367,332.961994112834));
#39942=CARTESIAN_POINT('Ctrl Pts',(130.24490860957,4.41925039963531,332.837073976477));
#39943=CARTESIAN_POINT('Ctrl Pts',(130.237151499795,4.3571703505436,332.714602855877));
#39944=CARTESIAN_POINT('Ctrl Pts',(130.229394390021,4.2901405083497,332.595030669402));
#39945=CARTESIAN_POINT('Ctrl Pts',(130.221633135095,4.2230748475513,332.475394587374));
#39946=CARTESIAN_POINT('Ctrl Pts',(130.213871880168,4.15105432836077,332.358660858676));
#39947=CARTESIAN_POINT('Ctrl Pts',(130.206110625242,4.07437595565987,332.245250712961));
#39948=CARTESIAN_POINT('Ctrl Pts',(130.198336954837,3.99757492255209,332.131659147973));
#39949=CARTESIAN_POINT('Ctrl Pts',(130.190563284433,3.91610137895022,332.021402104734));
#39950=CARTESIAN_POINT('Ctrl Pts',(130.182789614028,3.83029344536577,331.91486869244));
#39951=CARTESIAN_POINT('Ctrl Pts',(130.175377809851,3.74847989173427,331.813294436119));
#39952=CARTESIAN_POINT('Ctrl Pts',(130.167966005674,3.66272658791024,331.715105159063));
#39953=CARTESIAN_POINT('Ctrl Pts',(130.160554201497,3.57335667036554,331.620605798541));
#39954=CARTESIAN_POINT('Ctrl Pts',(130.152779122719,3.47960646694233,331.521474742861));
#39955=CARTESIAN_POINT('Ctrl Pts',(130.14500404394,3.38157989571606,331.42609118465));
#39956=CARTESIAN_POINT('Ctrl Pts',(130.137228965162,3.27960859023327,331.334846448323));
#39957=CARTESIAN_POINT('Ctrl Pts',(130.129463454113,3.17776276693348,331.243713994454));
#39958=CARTESIAN_POINT('Ctrl Pts',(130.121697943064,3.07198215643688,331.156710486845));
#39959=CARTESIAN_POINT('Ctrl Pts',(130.113932432015,2.96263701130687,331.074192439544));
#39960=CARTESIAN_POINT('Ctrl Pts',(130.106174620492,2.8534002822066,330.991756209127));
#39961=CARTESIAN_POINT('Ctrl Pts',(130.09841680897,2.74060636181404,330.913796822482));
#39962=CARTESIAN_POINT('Ctrl Pts',(130.090658997448,2.62466027155475,330.840632076695));
#39963=CARTESIAN_POINT('Ctrl Pts',(130.082907023925,2.50880143440497,330.767522389698));
#39964=CARTESIAN_POINT('Ctrl Pts',(130.075155050402,2.3897954781847,330.699200369527));
#39965=CARTESIAN_POINT('Ctrl Pts',(130.067403076879,2.2680779452533,330.635941625418));
#39966=CARTESIAN_POINT('Ctrl Pts',(130.059654386321,2.14641195976986,330.572709671426));
#39967=CARTESIAN_POINT('Ctrl Pts',(130.051905695764,2.0220370276797,330.514536908512));
#39968=CARTESIAN_POINT('Ctrl Pts',(130.044157005206,1.89541474203446,330.461653823453));
#39969=CARTESIAN_POINT('Ctrl Pts',(130.036409926828,1.76881880121349,330.408781741162));
#39970=CARTESIAN_POINT('Ctrl Pts',(130.02866284845,1.63997679734376,330.361197298172));
#39971=CARTESIAN_POINT('Ctrl Pts',(130.020915770073,1.50937146181384,330.319083332));
#39972=CARTESIAN_POINT('Ctrl Pts',(130.013168626767,1.37876503168533,330.276969012872));
#39973=CARTESIAN_POINT('Ctrl Pts',(130.005421483461,1.24639561243237,330.240325381966));
#39974=CARTESIAN_POINT('Ctrl Pts',(129.997674340155,1.11276191606658,330.209285650276));
#39975=CARTESIAN_POINT('Ctrl Pts',(129.989925455127,0.979098176008767,330.178238940195));
#39976=CARTESIAN_POINT('Ctrl Pts',(129.982176570099,0.844169973903678,330.152798724761));
#39977=CARTESIAN_POINT('Ctrl Pts',(129.974427685071,0.708486660083692,330.133047183814));
#39978=CARTESIAN_POINT('Ctrl Pts',(129.966670575296,0.572659330592638,330.113274678377));
#39979=CARTESIAN_POINT('Ctrl Pts',(129.958913465521,0.436075675756878,330.099202965329));
#39980=CARTESIAN_POINT('Ctrl Pts',(129.951156355747,0.299251179407041,330.090862418497));
#39981=CARTESIAN_POINT('Ctrl Pts',(129.943395100821,0.162353568421154,330.082517414743));
#39982=CARTESIAN_POINT('Ctrl Pts',(129.935633845894,0.0252152500842124,
330.079909687043));
#39983=CARTESIAN_POINT('Ctrl Pts',(129.927872590968,-0.111648828219296,
330.083017429189));
#39984=CARTESIAN_POINT('Ctrl Pts',(129.920098920564,-0.248731844444331,
330.08613014271));
#39985=CARTESIAN_POINT('Ctrl Pts',(129.912325250159,-0.385539353729229,
330.094976571042));
#39986=CARTESIAN_POINT('Ctrl Pts',(129.904551579754,-0.521561169438464,
330.109482950747));
#39987=CARTESIAN_POINT('Ctrl Pts',(129.897139775577,-0.651251136900461,
330.123314054987));
#39988=CARTESIAN_POINT('Ctrl Pts',(129.8897279714,-0.780226627975906,330.142289985724));
#39989=CARTESIAN_POINT('Ctrl Pts',(129.882316167223,-0.908056346721781,
330.16630402966));
#39990=CARTESIAN_POINT('Ctrl Pts',(129.874541088445,-1.04215138076962,330.191495073424));
#39991=CARTESIAN_POINT('Ctrl Pts',(129.866766009666,-1.17540925224237,330.222310192018));
#39992=CARTESIAN_POINT('Ctrl Pts',(129.858990930888,-1.30732142214948,330.258682275813));
#39993=CARTESIAN_POINT('Ctrl Pts',(129.851225419839,-1.43907126573354,330.295009601443));
#39994=CARTESIAN_POINT('Ctrl Pts',(129.84345990879,-1.56947832944978,330.336880183313));
#39995=CARTESIAN_POINT('Ctrl Pts',(129.835694397741,-1.69804244812341,330.38417559835));
#39996=CARTESIAN_POINT('Ctrl Pts',(129.827936586219,-1.82647909509925,330.431424119845));
#39997=CARTESIAN_POINT('Ctrl Pts',(129.820178774696,-1.95307606895754,330.484086636434));
#39998=CARTESIAN_POINT('Ctrl Pts',(129.812420963174,-2.07734694701626,330.541994535196));
#39999=CARTESIAN_POINT('Ctrl Pts',(129.804668989651,-2.20152430729843,330.599858856428));
#40000=CARTESIAN_POINT('Ctrl Pts',(129.796917016128,-2.32337870311768,330.662960538463));
#40001=CARTESIAN_POINT('Ctrl Pts',(129.789165042605,-2.44244267182418,330.731082472412));
#40002=CARTESIAN_POINT('Ctrl Pts',(129.781416352048,-2.5614562168692,330.79917555668));
#40003=CARTESIAN_POINT('Ctrl Pts',(129.77366766149,-2.67768134665106,330.872284470533));
#40004=CARTESIAN_POINT('Ctrl Pts',(129.765918970932,-2.79067444543647,330.950145780144));
#40005=CARTESIAN_POINT('Ctrl Pts',(129.758171892554,-2.90364403506375,331.027990890059));
#40006=CARTESIAN_POINT('Ctrl Pts',(129.750424814177,-3.01338260959016,331.11058620734));
#40007=CARTESIAN_POINT('Ctrl Pts',(129.742677735799,-3.1194751833941,331.197624736735));
#40008=CARTESIAN_POINT('Ctrl Pts',(129.734930592493,-3.22556864635589,331.284663995597));
#40009=CARTESIAN_POINT('Ctrl Pts',(129.727183449187,-3.32801574545603,331.37614629293));
#40010=CARTESIAN_POINT('Ctrl Pts',(129.719436305881,-3.4264345790412,331.471724339277));
#40011=CARTESIAN_POINT('Ctrl Pts',(129.711687420853,-3.52487553926979,331.567323873598));
#40012=CARTESIAN_POINT('Ctrl Pts',(129.703938535825,-3.61928615150944,331.667020716984));
#40013=CARTESIAN_POINT('Ctrl Pts',(129.696189650797,-3.70932167028769,331.770431018103));
#40014=CARTESIAN_POINT('Ctrl Pts',(129.688432541022,-3.79945275369569,331.873951079983));
#40015=CARTESIAN_POINT('Ctrl Pts',(129.680675431248,-3.88519921020425,331.981192177854));
#40016=CARTESIAN_POINT('Ctrl Pts',(129.672918321473,-3.96625653993615,332.091737267386));
#40017=CARTESIAN_POINT('Ctrl Pts',(129.665157066547,-4.0473571841136,332.202341428679));
#40018=CARTESIAN_POINT('Ctrl Pts',(129.657395811621,-4.12376349101779,332.316252775197));
#40019=CARTESIAN_POINT('Ctrl Pts',(129.649634556695,-4.19521513037563,332.433026476107));
#40020=CARTESIAN_POINT('Ctrl Pts',(129.64186088629,-4.26678106907022,332.549986976882));
#40021=CARTESIAN_POINT('Ctrl Pts',(129.634087215885,-4.33337631204293,332.669818640078));
#40022=CARTESIAN_POINT('Ctrl Pts',(129.626313545481,-4.39478679727931,332.792052521241));
#40023=CARTESIAN_POINT('Ctrl Pts',(129.618901741304,-4.45333860965332,332.908596385827));
#40024=CARTESIAN_POINT('Ctrl Pts',(129.611489937126,-4.50717738349597,333.027323592805));
#40025=CARTESIAN_POINT('Ctrl Pts',(129.604078132949,-4.55615945731404,333.147813707526));
#40026=CARTESIAN_POINT('Ctrl Pts',(129.595116309249,-4.61538507897874,333.29350173975));
#40027=CARTESIAN_POINT('Ctrl Pts',(129.586154485548,-4.66767254577,333.442165238511));
#40028=CARTESIAN_POINT('Ctrl Pts',(129.577192661848,-4.71274877049981,333.593165934215));
#40029=CARTESIAN_POINT('Ctrl Pts',(129.568494161544,-4.75650052992046,333.739729807974));
#40030=CARTESIAN_POINT('Ctrl Pts',(129.55979566124,-4.79345868248545,333.888495249248));
#40031=CARTESIAN_POINT('Ctrl Pts',(129.551097160936,-4.82342038277065,334.038855435654));
#40032=CARTESIAN_POINT('Ctrl Pts',(129.542003675537,-4.85474259631828,334.196043239511));
#40033=CARTESIAN_POINT('Ctrl Pts',(129.532910190138,-4.87841796184014,334.354973856826));
#40034=CARTESIAN_POINT('Ctrl Pts',(129.52381670474,-4.8942712126928,334.514930562593));
#40035=CARTESIAN_POINT('Ctrl Pts',(129.515189481392,-4.90931159928784,334.666685601074));
#40036=CARTESIAN_POINT('Ctrl Pts',(129.506562258044,-4.91731175971941,334.819363839407));
#40037=CARTESIAN_POINT('Ctrl Pts',(129.497935034696,-4.91817219910754,334.972336261538));
#40038=CARTESIAN_POINT('Ctrl Pts',(129.497468772645,-4.91821870192979,334.980603722854));
#40039=CARTESIAN_POINT('Ctrl Pts',(129.497002510594,-4.91824436243081,334.988872039881));
#40040=CARTESIAN_POINT('Ctrl Pts',(129.496536248543,-4.91824916909057,334.997141112125));
#40041=CARTESIAN_POINT('',(132.996536248523,-4.91824810241123,335.004320373636));
#40042=CARTESIAN_POINT('Ctrl Pts',(132.99653624849,-4.91824810241071,335.004320374226));
#40043=CARTESIAN_POINT('Ctrl Pts',(132.985166312015,-4.91807204458086,335.204741921598));
#40044=CARTESIAN_POINT('Ctrl Pts',(132.973796375539,-4.90564181988563,335.404646016326));
#40045=CARTESIAN_POINT('Ctrl Pts',(132.962426439064,-4.88116543082435,335.602832563342));
#40046=CARTESIAN_POINT('Ctrl Pts',(132.955929140788,-4.86717851007207,335.716085360572));
#40047=CARTESIAN_POINT('Ctrl Pts',(132.949431842512,-4.84925871495562,335.828778013465));
#40048=CARTESIAN_POINT('Ctrl Pts',(132.942934544237,-4.82745109785408,335.940690682598));
#40049=CARTESIAN_POINT('Ctrl Pts',(132.935159465458,-4.80135472152312,336.07461247315));
#40050=CARTESIAN_POINT('Ctrl Pts',(132.92738438668,-4.76964005433339,336.207659125601));
#40051=CARTESIAN_POINT('Ctrl Pts',(132.919609307901,-4.73237763992542,336.339322565939));
#40052=CARTESIAN_POINT('Ctrl Pts',(132.911843796852,-4.69516107929066,336.470823986032));
#40053=CARTESIAN_POINT('Ctrl Pts',(132.904078285803,-4.65241046034805,336.600945208256));
#40054=CARTESIAN_POINT('Ctrl Pts',(132.896312774754,-4.6042475824392,336.729186878883));
#40055=CARTESIAN_POINT('Ctrl Pts',(132.888554963232,-4.55613245816402,336.857301397521));
#40056=CARTESIAN_POINT('Ctrl Pts',(132.88079715171,-4.50261589064495,336.983539709631));
#40057=CARTESIAN_POINT('Ctrl Pts',(132.873039340188,-4.44386977508548,337.107416542732));
#40058=CARTESIAN_POINT('Ctrl Pts',(132.865287366665,-4.38516786784091,337.231200154588));
#40059=CARTESIAN_POINT('Ctrl Pts',(132.857535393142,-4.32124441258973,337.35262547289));
#40060=CARTESIAN_POINT('Ctrl Pts',(132.849783419619,-4.25231967130944,337.471226512381));
#40061=CARTESIAN_POINT('Ctrl Pts',(132.842034729061,-4.18342411969796,337.589777324261));
#40062=CARTESIAN_POINT('Ctrl Pts',(132.834286038504,-4.10953169069499,337.705505899011));
#40063=CARTESIAN_POINT('Ctrl Pts',(132.826537347946,-4.03090880905422,337.817970410701));
#40064=CARTESIAN_POINT('Ctrl Pts',(132.818790269568,-3.95230228556062,337.930411523211));
#40065=CARTESIAN_POINT('Ctrl Pts',(132.81104319119,-3.86896749090839,338.03958960332));
#40066=CARTESIAN_POINT('Ctrl Pts',(132.803296112813,-3.78121421686721,338.145091748846));
#40067=CARTESIAN_POINT('Ctrl Pts',(132.795548969507,-3.69346020736914,338.250594778582));
#40068=CARTESIAN_POINT('Ctrl Pts',(132.787801826201,-3.60128789457463,338.352421511779));
#40069=CARTESIAN_POINT('Ctrl Pts',(132.780054682895,-3.50504714003312,338.450192401685));
#40070=CARTESIAN_POINT('Ctrl Pts',(132.772305797867,-3.4087847485269,338.547985272563));
#40071=CARTESIAN_POINT('Ctrl Pts',(132.764556912839,-3.30845236932635,338.641720207185));
#40072=CARTESIAN_POINT('Ctrl Pts',(132.756808027811,-3.20443617400694,338.731055061134));
#40073=CARTESIAN_POINT('Ctrl Pts',(132.749050918036,-3.10030957482292,338.820484736021));
#40074=CARTESIAN_POINT('Ctrl Pts',(132.741293808261,-2.99249164583852,338.905504745818));
#40075=CARTESIAN_POINT('Ctrl Pts',(132.733536698487,-2.88140147898083,338.985813415029));
#40076=CARTESIAN_POINT('Ctrl Pts',(132.725775443561,-2.77025194908991,339.066164998625));
#40077=CARTESIAN_POINT('Ctrl Pts',(132.718014188634,-2.65582702303574,339.141800009682));
#40078=CARTESIAN_POINT('Ctrl Pts',(132.710252933708,-2.53857328021474,339.212461129017));
#40079=CARTESIAN_POINT('Ctrl Pts',(132.702479263304,-2.4211319696182,339.283235283114));
#40080=CARTESIAN_POINT('Ctrl Pts',(132.694705592899,-2.30085314270943,339.349019458175));
#40081=CARTESIAN_POINT('Ctrl Pts',(132.686931922494,-2.1782071793833,339.409602765123));
#40082=CARTESIAN_POINT('Ctrl Pts',(132.679520118317,-2.06127041515641,339.467365904558));
#40083=CARTESIAN_POINT('Ctrl Pts',(132.67210831414,-1.9421821982926,339.520401362981));
#40084=CARTESIAN_POINT('Ctrl Pts',(132.664696509963,-1.821363924382,339.568568322512));
#40085=CARTESIAN_POINT('Ctrl Pts',(132.656921431184,-1.69462398696847,339.619096088212));
#40086=CARTESIAN_POINT('Ctrl Pts',(132.649146352406,-1.56557959229293,339.664425725826));
#40087=CARTESIAN_POINT('Ctrl Pts',(132.641371273628,-1.4346961658433,339.704341609005));
#40088=CARTESIAN_POINT('Ctrl Pts',(132.633605762579,-1.30397379978233,339.744208373149));
#40089=CARTESIAN_POINT('Ctrl Pts',(132.62584025153,-1.17141727505926,339.778674525335));
#40090=CARTESIAN_POINT('Ctrl Pts',(132.618074740481,-1.0375124214905,339.807572260274));
#40091=CARTESIAN_POINT('Ctrl Pts',(132.610316928958,-0.903740334973862,
339.836441343024));
#40092=CARTESIAN_POINT('Ctrl Pts',(132.602559117436,-0.768622959679355,
339.859752913907));
#40093=CARTESIAN_POINT('Ctrl Pts',(132.594801305914,-0.632661393947455,
339.877388914482));
#40094=CARTESIAN_POINT('Ctrl Pts',(132.587049332391,-0.496802143605495,
339.895011643407));
#40095=CARTESIAN_POINT('Ctrl Pts',(132.579297358868,-0.360100353386185,
339.906967253255));
#40096=CARTESIAN_POINT('Ctrl Pts',(132.571545385345,-0.223067076628279,
339.913188795663));
#40097=CARTESIAN_POINT('Ctrl Pts',(132.563796694787,-0.0860918335444363,
339.919407703243));
#40098=CARTESIAN_POINT('Ctrl Pts',(132.55604800423,0.0512142272032169,339.919897355569));
#40099=CARTESIAN_POINT('Ctrl Pts',(132.548299313672,0.188335387045108,339.91464269754));
#40100=CARTESIAN_POINT('Ctrl Pts',(132.540552235294,0.325428017684436,339.909389132787));
#40101=CARTESIAN_POINT('Ctrl Pts',(132.532805156916,0.462335433595527,339.898393649877));
#40102=CARTESIAN_POINT('Ctrl Pts',(132.525058078539,0.598542770423849,339.881693314258));
#40103=CARTESIAN_POINT('Ctrl Pts',(132.517310935233,0.734751248800706,339.864992838674));
#40104=CARTESIAN_POINT('Ctrl Pts',(132.509563791927,0.870259248422978,339.842587462585));
#40105=CARTESIAN_POINT('Ctrl Pts',(132.501816648621,1.00455827017125,339.814565997505));
#40106=CARTESIAN_POINT('Ctrl Pts',(132.494067763593,1.13888748519099,339.786538232605));
#40107=CARTESIAN_POINT('Ctrl Pts',(132.486318878565,1.27200679891804,339.752891946071));
#40108=CARTESIAN_POINT('Ctrl Pts',(132.478569993537,1.40341951521538,339.713766723843));
#40109=CARTESIAN_POINT('Ctrl Pts',(132.470812883762,1.53497171432755,339.674599973701));
#40110=CARTESIAN_POINT('Ctrl Pts',(132.463055773987,1.66481332235345,339.629942782771));
#40111=CARTESIAN_POINT('Ctrl Pts',(132.455298664213,1.79246385924236,339.579984320476));
#40112=CARTESIAN_POINT('Ctrl Pts',(132.447537409287,1.92018260849663,339.529999161977));
#40113=CARTESIAN_POINT('Ctrl Pts',(132.43977615436,2.04570759608539,339.474707244928));
#40114=CARTESIAN_POINT('Ctrl Pts',(132.432014899434,2.16858076708155,339.414344857297));
#40115=CARTESIAN_POINT('Ctrl Pts',(132.42424122903,2.29165049510703,339.353885909518));
#40116=CARTESIAN_POINT('Ctrl Pts',(132.416467558625,2.41205958619735,339.288340469755));
#40117=CARTESIAN_POINT('Ctrl Pts',(132.40869388822,2.52937614967794,339.217989966316));
#40118=CARTESIAN_POINT('Ctrl Pts',(132.401282084043,2.64123159890342,339.150914295738));
#40119=CARTESIAN_POINT('Ctrl Pts',(132.393870279866,2.75027571477758,339.079471003268));
#40120=CARTESIAN_POINT('Ctrl Pts',(132.386458475689,2.85616203920789,339.003938244814));
#40121=CARTESIAN_POINT('Ctrl Pts',(132.378683396911,2.96723816781801,338.924703400868));
#40122=CARTESIAN_POINT('Ctrl Pts',(132.370908318132,3.07519015367777,338.840717684271));
#40123=CARTESIAN_POINT('Ctrl Pts',(132.363133239354,3.17958480355244,338.752255793455));
#40124=CARTESIAN_POINT('Ctrl Pts',(132.355367728305,3.28385098916439,338.663902760628));
#40125=CARTESIAN_POINT('Ctrl Pts',(132.347602217256,3.38456825346058,338.571084763634));
#40126=CARTESIAN_POINT('Ctrl Pts',(132.339836706207,3.48133257500152,338.47411953806));
#40127=CARTESIAN_POINT('Ctrl Pts',(132.332078894684,3.57800095443589,338.37725045379));
#40128=CARTESIAN_POINT('Ctrl Pts',(132.324321083162,3.67072391652706,338.276242598925));
#40129=CARTESIAN_POINT('Ctrl Pts',(132.31656327164,3.75913101034844,338.171453469552));
#40130=CARTESIAN_POINT('Ctrl Pts',(132.308811298117,3.84747157502812,338.066743197323));
#40131=CARTESIAN_POINT('Ctrl Pts',(132.301059324594,3.93150248504629,337.958257612025));
#40132=CARTESIAN_POINT('Ctrl Pts',(132.293307351071,4.01089088180881,337.846390239711));
#40133=CARTESIAN_POINT('Ctrl Pts',(132.285558660513,4.09024565753819,337.734570243296));
#40134=CARTESIAN_POINT('Ctrl Pts',(132.277809969956,4.16496160471648,337.619371626487));
#40135=CARTESIAN_POINT('Ctrl Pts',(132.270061279398,4.23474697827753,337.501219920852));
#40136=CARTESIAN_POINT('Ctrl Pts',(132.26231420102,4.30451783240876,337.383092797667));
#40137=CARTESIAN_POINT('Ctrl Pts',(132.254567122642,4.36935995474722,337.262014144113));
#40138=CARTESIAN_POINT('Ctrl Pts',(132.246820044265,4.4290258917723,337.138436978849));
#40139=CARTESIAN_POINT('Ctrl Pts',(132.239072900959,4.48869232885536,337.01485877789));
#40140=CARTESIAN_POINT('Ctrl Pts',(132.231325757653,4.54318232414685,336.888782375449));
#40141=CARTESIAN_POINT('Ctrl Pts',(132.223578614347,4.59229538309382,336.760683440291));
#40142=CARTESIAN_POINT('Ctrl Pts',(132.215829729319,4.64141948369911,336.632555705773));
#40143=CARTESIAN_POINT('Ctrl Pts',(132.208080844291,4.68516410258287,336.502404898617));
#40144=CARTESIAN_POINT('Ctrl Pts',(132.200331959263,4.72337782976025,336.370724239163));
#40145=CARTESIAN_POINT('Ctrl Pts',(132.192574849488,4.76163211738251,336.238903812497));
#40146=CARTESIAN_POINT('Ctrl Pts',(132.184817739713,4.79434367722345,336.105550665818));
#40147=CARTESIAN_POINT('Ctrl Pts',(132.177060629939,4.82141157055939,335.97117121548));
#40148=CARTESIAN_POINT('Ctrl Pts',(132.169299375013,4.84849392811207,335.83671995706));
#40149=CARTESIAN_POINT('Ctrl Pts',(132.161538120086,4.86992654887105,335.701241688073));
#40150=CARTESIAN_POINT('Ctrl Pts',(132.15377686516,4.88566025262429,335.565249465658));
#40151=CARTESIAN_POINT('Ctrl Pts',(132.146003194756,4.90141912517593,335.429039700007));
#40152=CARTESIAN_POINT('Ctrl Pts',(132.138229524351,4.91146083478947,335.292314728042));
#40153=CARTESIAN_POINT('Ctrl Pts',(132.130455853946,4.91578831970801,335.15559003285));
#40154=CARTESIAN_POINT('Ctrl Pts',(132.123044049769,4.91991435916246,335.025229905114));
#40155=CARTESIAN_POINT('Ctrl Pts',(132.115632245592,4.91884619839865,334.89487031675));
#40156=CARTESIAN_POINT('Ctrl Pts',(132.108220441415,4.91263025629944,334.764953137883));
#40157=CARTESIAN_POINT('Ctrl Pts',(132.100445362637,4.90610965236161,334.628668331075));
#40158=CARTESIAN_POINT('Ctrl Pts',(132.092670283858,4.89390328535079,334.492439712761));
#40159=CARTESIAN_POINT('Ctrl Pts',(132.08489520508,4.87600772932303,334.356780219457));
#40160=CARTESIAN_POINT('Ctrl Pts',(132.077129694031,4.85813419491626,334.221287663795));
#40161=CARTESIAN_POINT('Ctrl Pts',(132.069364182982,4.83458545192537,334.086363223471));
#40162=CARTESIAN_POINT('Ctrl Pts',(132.061598671933,4.80541005179943,333.95251859369));
#40163=CARTESIAN_POINT('Ctrl Pts',(132.05384086041,4.77626357916766,333.818806671249));
#40164=CARTESIAN_POINT('Ctrl Pts',(132.046083048888,4.74150163433323,333.686172808172));
#40165=CARTESIAN_POINT('Ctrl Pts',(132.038325237366,4.7012243711309,333.555121986192));
#40166=CARTESIAN_POINT('Ctrl Pts',(132.030573263843,4.66097741784642,333.424169784113));
#40167=CARTESIAN_POINT('Ctrl Pts',(132.02282129032,4.61522352183404,333.294798624051));
#40168=CARTESIAN_POINT('Ctrl Pts',(132.015069316797,4.56411347866309,333.167501373429));
#40169=CARTESIAN_POINT('Ctrl Pts',(132.007320626239,4.51302508062575,333.040258033268));
#40170=CARTESIAN_POINT('Ctrl Pts',(131.999571935682,4.45658519231475,332.91508721764));
#40171=CARTESIAN_POINT('Ctrl Pts',(131.991823245124,4.39499377230843,332.792464540745));
#40172=CARTESIAN_POINT('Ctrl Pts',(131.984076166746,4.33341516691146,332.669867376521));
#40173=CARTESIAN_POINT('Ctrl Pts',(131.976329088368,4.26668733707546,332.549817645571));
#40174=CARTESIAN_POINT('Ctrl Pts',(131.968582009991,4.19505732455719,332.432768591229));
#40175=CARTESIAN_POINT('Ctrl Pts',(131.960834866685,4.12342671171045,332.315718555904));
#40176=CARTESIAN_POINT('Ctrl Pts',(131.953087723379,4.04689403826312,332.201669580747));
#40177=CARTESIAN_POINT('Ctrl Pts',(131.945340580073,3.96575080512067,332.091047677568));
#40178=CARTESIAN_POINT('Ctrl Pts',(131.937591695045,3.88458932925674,331.980400904236));
#40179=CARTESIAN_POINT('Ctrl Pts',(131.929842810017,3.79881546221727,331.873183051162));
#40180=CARTESIAN_POINT('Ctrl Pts',(131.922093924989,3.70876202687786,331.76978835206));
#40181=CARTESIAN_POINT('Ctrl Pts',(131.914336815214,3.61861300789172,331.666283908755));
#40182=CARTESIAN_POINT('Ctrl Pts',(131.90657970544,3.5241756039036,331.566611020744));
#40183=CARTESIAN_POINT('Ctrl Pts',(131.898822595665,3.42582104749373,331.471128620501));
#40184=CARTESIAN_POINT('Ctrl Pts',(131.891061340739,3.32741393355371,331.375595197515));
#40185=CARTESIAN_POINT('Ctrl Pts',(131.883300085812,3.2250857877574,331.284256984384));
#40186=CARTESIAN_POINT('Ctrl Pts',(131.875538830886,3.1192414365625,331.197432982454));
#40187=CARTESIAN_POINT('Ctrl Pts',(131.867765160482,3.01322776890029,331.110470090416));
#40188=CARTESIAN_POINT('Ctrl Pts',(131.859991490077,2.90368696834014,331.028036074963));
#40189=CARTESIAN_POINT('Ctrl Pts',(131.852217819672,2.79105410566051,330.950407422743));
#40190=CARTESIAN_POINT('Ctrl Pts',(131.844806015495,2.68366432983633,330.87639240296));
#40191=CARTESIAN_POINT('Ctrl Pts',(131.837394211318,2.57346412780097,330.806745588839));
#40192=CARTESIAN_POINT('Ctrl Pts',(131.829982407141,2.46085019748905,330.74166706703));
#40193=CARTESIAN_POINT('Ctrl Pts',(131.822207328363,2.342716722993,330.673398853008));
#40194=CARTESIAN_POINT('Ctrl Pts',(131.814432249584,2.22155360595167,330.609942325273));
#40195=CARTESIAN_POINT('Ctrl Pts',(131.806657170806,2.0977903316501,330.551577944154));
#40196=CARTESIAN_POINT('Ctrl Pts',(131.798891659757,1.97417935593668,330.493285384122));
#40197=CARTESIAN_POINT('Ctrl Pts',(131.791126148708,1.84797493952248,330.440072667872));
#40198=CARTESIAN_POINT('Ctrl Pts',(131.783360637659,1.71963365179694,330.392175875089));
#40199=CARTESIAN_POINT('Ctrl Pts',(131.775602826136,1.59141961483201,330.344326572117));
#40200=CARTESIAN_POINT('Ctrl Pts',(131.767845014614,1.4610732867611,330.301782839301));
#40201=CARTESIAN_POINT('Ctrl Pts',(131.760087203092,1.32907351648444,330.264733729738));
#40202=CARTESIAN_POINT('Ctrl Pts',(131.752335229569,1.19717308022083,330.227712500805));
#40203=CARTESIAN_POINT('Ctrl Pts',(131.744583256046,1.06362205322197,330.196177770053));
#40204=CARTESIAN_POINT('Ctrl Pts',(131.736831282523,0.928916502352443,330.170269449114));
#40205=CARTESIAN_POINT('Ctrl Pts',(131.729082591965,0.794267999363639,330.144372100365));
#40206=CARTESIAN_POINT('Ctrl Pts',(131.721333901408,0.658466328014882,330.124096495902));
#40207=CARTESIAN_POINT('Ctrl Pts',(131.71358521085,0.522019651493034,330.109531868425));
#40208=CARTESIAN_POINT('Ctrl Pts',(131.705838132472,0.385601363841908,330.09497027124));
#40209=CARTESIAN_POINT('Ctrl Pts',(131.698091054094,0.248538726370752,330.086117329055));
#40210=CARTESIAN_POINT('Ctrl Pts',(131.690343975717,0.111346569539857,330.083010575164));
#40211=CARTESIAN_POINT('Ctrl Pts',(131.682596832411,-0.0258467370934059,
330.079903795234));
#40212=CARTESIAN_POINT('Ctrl Pts',(131.674849689105,-0.163169174477405,
330.082543308503));
#40213=CARTESIAN_POINT('Ctrl Pts',(131.667102545799,-0.300104752326663,
330.090914525074));
#40214=CARTESIAN_POINT('Ctrl Pts',(131.659353660771,-0.437071116201,330.099287623672));
#40215=CARTESIAN_POINT('Ctrl Pts',(131.651604775743,-0.573650057401876,
330.113394965913));
#40216=CARTESIAN_POINT('Ctrl Pts',(131.643855890715,-0.70932994683372,330.133170016425));
#40217=CARTESIAN_POINT('Ctrl Pts',(131.63609878094,-0.845153848302135,330.15296605638));
#40218=CARTESIAN_POINT('Ctrl Pts',(131.628341671165,-0.980076404373335,
330.178441765195));
#40219=CARTESIAN_POINT('Ctrl Pts',(131.620584561391,-1.11359488582268,330.209479204432));
#40220=CARTESIAN_POINT('Ctrl Pts',(131.612823306464,-1.24718471527936,330.240533229084));
#40221=CARTESIAN_POINT('Ctrl Pts',(131.605062051538,-1.37936859859475,330.277154801849));
#40222=CARTESIAN_POINT('Ctrl Pts',(131.597300796612,-1.5096592059064,330.319176125454));
#40223=CARTESIAN_POINT('Ctrl Pts',(131.589527126207,-1.64015823572809,330.361264669482));
#40224=CARTESIAN_POINT('Ctrl Pts',(131.581753455803,-1.7687575706075,330.4087700898));
#40225=CARTESIAN_POINT('Ctrl Pts',(131.573979785398,-1.89498926526261,330.461476148896));
#40226=CARTESIAN_POINT('Ctrl Pts',(131.566567981221,-2.01534484416103,330.511728728261));
#40227=CARTESIAN_POINT('Ctrl Pts',(131.559156177044,-2.13354798861138,330.566708541716));
#40228=CARTESIAN_POINT('Ctrl Pts',(131.551744372867,-2.24921576546666,330.626190275872));
#40229=CARTESIAN_POINT('Ctrl Pts',(131.543969294089,-2.37055276462297,330.688587387006));
#40230=CARTESIAN_POINT('Ctrl Pts',(131.53619421531,-2.48948302755049,330.756136068736));
#40231=CARTESIAN_POINT('Ctrl Pts',(131.528419136532,-2.60553829004209,330.828626930899));
#40232=CARTESIAN_POINT('Ctrl Pts',(131.520653625483,-2.72145073914472,330.901028588441));
#40233=CARTESIAN_POINT('Ctrl Pts',(131.512888114434,-2.83449489881281,330.978360120548));
#40234=CARTESIAN_POINT('Ctrl Pts',(131.505122603385,-2.94422516870629,331.060365344546));
#40235=CARTESIAN_POINT('Ctrl Pts',(131.497364791862,-3.05384664071762,331.142289260125));
#40236=CARTESIAN_POINT('Ctrl Pts',(131.48960698034,-3.16016045066288,331.228877413231));
#40237=CARTESIAN_POINT('Ctrl Pts',(131.481849168818,-3.2627484871443,331.319829437086));
#40238=CARTESIAN_POINT('Ctrl Pts',(131.474097195295,-3.36525932287509,331.410713016659));
#40239=CARTESIAN_POINT('Ctrl Pts',(131.466345221772,-3.46404967459343,331.505953672176));
#40240=CARTESIAN_POINT('Ctrl Pts',(131.458593248249,-3.55873343737917,331.60520996464));
#40241=CARTESIAN_POINT('Ctrl Pts',(131.450844557691,-3.65337710153515,331.704424222005));
#40242=CARTESIAN_POINT('Ctrl Pts',(131.443095867134,-3.7439173665542,331.807650451655));
#40243=CARTESIAN_POINT('Ctrl Pts',(131.435347176576,-3.83000419849704,331.914509617258));
#40244=CARTESIAN_POINT('Ctrl Pts',(131.427600098198,-3.91607311935545,332.021346549919));
#40245=CARTESIAN_POINT('Ctrl Pts',(131.419853019821,-3.99769020509566,332.131814610874));
#40246=CARTESIAN_POINT('Ctrl Pts',(131.412105941443,-4.07454528886835,332.245501179623));
#40247=CARTESIAN_POINT('Ctrl Pts',(131.404358798137,-4.15140101676064,332.359188701174));
#40248=CARTESIAN_POINT('Ctrl Pts',(131.396611654831,-4.22349444416985,332.476094460501));
#40249=CARTESIAN_POINT('Ctrl Pts',(131.388864511525,-4.29055860809946,332.595776654933));
#40250=CARTESIAN_POINT('Ctrl Pts',(131.381115626497,-4.35763784947678,332.715485756464));
#40251=CARTESIAN_POINT('Ctrl Pts',(131.373366741469,-4.41968538640075,332.837972194269));
#40252=CARTESIAN_POINT('Ctrl Pts',(131.365617856441,-4.47648029802522,332.962769722419));
#40253=CARTESIAN_POINT('Ctrl Pts',(131.357860746666,-4.53333549235583,333.087699711956));
#40254=CARTESIAN_POINT('Ctrl Pts',(131.350103636892,-4.58492676225724,333.214945335638));
#40255=CARTESIAN_POINT('Ctrl Pts',(131.342346527117,-4.63108122904954,333.344020014479));
#40256=CARTESIAN_POINT('Ctrl Pts',(131.334585272191,-4.67726035931314,333.473163666702));
#40257=CARTESIAN_POINT('Ctrl Pts',(131.326824017265,-4.71799678146001,333.604137948569));
#40258=CARTESIAN_POINT('Ctrl Pts',(131.319062762338,-4.75316787764475,333.736442249271));
#40259=CARTESIAN_POINT('Ctrl Pts',(131.311289091934,-4.78839523612117,333.868958193737));
#40260=CARTESIAN_POINT('Ctrl Pts',(131.303515421529,-4.81803939382419,334.002808026778));
#40261=CARTESIAN_POINT('Ctrl Pts',(131.295741751124,-4.84202895744665,334.137481224698));
#40262=CARTESIAN_POINT('Ctrl Pts',(131.288329946947,-4.86490180111146,334.265885352858));
#40263=CARTESIAN_POINT('Ctrl Pts',(131.28091814277,-4.88263460699182,334.395037630585));
#40264=CARTESIAN_POINT('Ctrl Pts',(131.273506338593,-4.89520961882523,334.524494111224));
#40265=CARTESIAN_POINT('Ctrl Pts',(131.264516308558,-4.91046227949477,334.681516291147));
#40266=CARTESIAN_POINT('Ctrl Pts',(131.255526278524,-4.91816144897856,334.83928396875));
#40267=CARTESIAN_POINT('Ctrl Pts',(131.24653624849,-4.91824924060749,334.997266913122));
#40268=CARTESIAN_POINT('',(134.746536248449,-4.91824997633412,335.000482482528));
#40269=CARTESIAN_POINT('Ctrl Pts',(134.746536248449,-4.91824997633412,335.000482482528));
#40270=CARTESIAN_POINT('Ctrl Pts',(134.73835890364,-4.91823573273552,335.145676503863));
#40271=CARTESIAN_POINT('Ctrl Pts',(134.730181558832,-4.91178769478722,335.290726823761));
#40272=CARTESIAN_POINT('Ctrl Pts',(134.722004214023,-4.89896956597948,335.435063505832));
#40273=CARTESIAN_POINT('Ctrl Pts',(134.713813828826,-4.88613099613821,335.579630361199));
#40274=CARTESIAN_POINT('Ctrl Pts',(134.705623443629,-4.86690208535552,335.723480987154));
#40275=CARTESIAN_POINT('Ctrl Pts',(134.697433058432,-4.84139785573774,335.866054192853));
#40276=CARTESIAN_POINT('Ctrl Pts',(134.689221195481,-4.81582674604515,336.009001270133));
#40277=CARTESIAN_POINT('Ctrl Pts',(134.68100933253,-4.78394746694061,336.150663910874));
#40278=CARTESIAN_POINT('Ctrl Pts',(134.672797469578,-4.74592579345992,336.290492706478));
#40279=CARTESIAN_POINT('Ctrl Pts',(134.664573976314,-4.70785027056847,336.430519539084));
#40280=CARTESIAN_POINT('Ctrl Pts',(134.656350483049,-4.66361508511763,336.568707036158));
#40281=CARTESIAN_POINT('Ctrl Pts',(134.648126989784,-4.61343476530339,336.704524194252));
#40282=CARTESIAN_POINT('Ctrl Pts',(134.639884397592,-4.5631379025238,336.840656785456));
#40283=CARTESIAN_POINT('Ctrl Pts',(134.6316418054,-4.50686842177647,336.974407733546));
#40284=CARTESIAN_POINT('Ctrl Pts',(134.623399213208,-4.44488829345144,337.105267470237));
#40285=CARTESIAN_POINT('Ctrl Pts',(134.619720392099,-4.41722541760802,337.163672587277));
#40286=CARTESIAN_POINT('Ctrl Pts',(134.616041570989,-4.38842557466354,337.221502133846));
#40287=CARTESIAN_POINT('Ctrl Pts',(134.61236274988,-4.35851485952536,337.27871263695));
#40288=CARTESIAN_POINT('Ctrl Pts',(134.604587671102,-4.29529945447882,337.399625330275));
#40289=CARTESIAN_POINT('Ctrl Pts',(134.596812592323,-4.22694885561345,337.518096539765));
#40290=CARTESIAN_POINT('Ctrl Pts',(134.589037513545,-4.15367561177011,337.63365942648));
#40291=CARTESIAN_POINT('Ctrl Pts',(134.581272002496,-4.08049253531808,337.749080105705));
#40292=CARTESIAN_POINT('Ctrl Pts',(134.573506491447,-4.0023990741382,337.861599256138));
#40293=CARTESIAN_POINT('Ctrl Pts',(134.565740980398,-3.91965441540698,337.970773018304));
#40294=CARTESIAN_POINT('Ctrl Pts',(134.557983168875,-3.83699179824588,338.079838534366));
#40295=CARTESIAN_POINT('Ctrl Pts',(134.550225357353,-3.74968739560838,338.185564953597));
#40296=CARTESIAN_POINT('Ctrl Pts',(134.542467545831,-3.65804439205829,338.287536203334));
#40297=CARTESIAN_POINT('Ctrl Pts',(134.534715572308,-3.56647035277456,338.389430716471));
#40298=CARTESIAN_POINT('Ctrl Pts',(134.526963598785,-3.4705644714938,338.487575395348));
#40299=CARTESIAN_POINT('Ctrl Pts',(134.519211625262,-3.37067078783581,338.581586450517));
#40300=CARTESIAN_POINT('Ctrl Pts',(134.511462934704,-3.27081940921213,338.67555769195));
#40301=CARTESIAN_POINT('Ctrl Pts',(134.503714244147,-3.16698387123994,338.765398524156));
#40302=CARTESIAN_POINT('Ctrl Pts',(134.495965553589,-3.05954556632937,338.850761481844));
#40303=CARTESIAN_POINT('Ctrl Pts',(134.488218475211,-2.95212961485544,338.936106679056));
#40304=CARTESIAN_POINT('Ctrl Pts',(134.480471396834,-2.84111269326651,339.016975611885));
#40305=CARTESIAN_POINT('Ctrl Pts',(134.472724318456,-2.72690950804375,339.093060908103));
#40306=CARTESIAN_POINT('Ctrl Pts',(134.46497717515,-2.61270536568846,339.169146841989));
#40307=CARTESIAN_POINT('Ctrl Pts',(134.457230031844,-2.49531523172932,339.240448842581));
#40308=CARTESIAN_POINT('Ctrl Pts',(134.449482888538,-2.37518270227838,339.306702937666));
#40309=CARTESIAN_POINT('Ctrl Pts',(134.44173400351,-2.25502316448436,339.372971928077));
#40310=CARTESIAN_POINT('Ctrl Pts',(134.433985118482,-2.13212034654061,339.434190565976));
#40311=CARTESIAN_POINT('Ctrl Pts',(134.426236233454,-2.00694197621473,339.490141085379));
#40312=CARTESIAN_POINT('Ctrl Pts',(134.418479123679,-1.88163074027313,339.546150991242));
#40313=CARTESIAN_POINT('Ctrl Pts',(134.410722013905,-1.75403948458573,339.596881449041));
#40314=CARTESIAN_POINT('Ctrl Pts',(134.40296490413,-1.62465594495468,339.64216287123));
#40315=CARTESIAN_POINT('Ctrl Pts',(134.395203649204,-1.49520326689706,339.687468490363));
#40316=CARTESIAN_POINT('Ctrl Pts',(134.387442394278,-1.36395677033809,339.727319158375));
#40317=CARTESIAN_POINT('Ctrl Pts',(134.379681139351,-1.23141788303495,339.761595642203));
#40318=CARTESIAN_POINT('Ctrl Pts',(134.371907468947,-1.09866697670641,339.795926957233));
#40319=CARTESIAN_POINT('Ctrl Pts',(134.364133798542,-0.964619930738429,
339.824666187533));
#40320=CARTESIAN_POINT('Ctrl Pts',(134.356360128137,-0.829787739488795,
339.847745390374));
#40321=CARTESIAN_POINT('Ctrl Pts',(134.34894832396,-0.701232019180494,339.869750250771));
#40322=CARTESIAN_POINT('Ctrl Pts',(134.341536519783,-0.571962890992541,
339.886610136396));
#40323=CARTESIAN_POINT('Ctrl Pts',(134.334124715606,-0.442424411406601,
339.898310290569));
#40324=CARTESIAN_POINT('Ctrl Pts',(134.326349636828,-0.30653686506098,339.91058390415));
#40325=CARTESIAN_POINT('Ctrl Pts',(134.318574558049,-0.169923466525491,
339.9172179967));
#40326=CARTESIAN_POINT('Ctrl Pts',(134.310799479271,-0.0330918129995932,
339.918138671735));
#40327=CARTESIAN_POINT('Ctrl Pts',(134.303033968222,0.103571460465418,339.91905821382));
#40328=CARTESIAN_POINT('Ctrl Pts',(134.295268457173,0.240452067401368,339.91427832491));
#40329=CARTESIAN_POINT('Ctrl Pts',(134.287502946124,0.37703649585296,339.903776763199));
#40330=CARTESIAN_POINT('Ctrl Pts',(134.279745134602,0.513485500446227,339.893285613818));
#40331=CARTESIAN_POINT('Ctrl Pts',(134.27198732308,0.64963852374524,339.87708411111));
#40332=CARTESIAN_POINT('Ctrl Pts',(134.264229511557,0.784981610805304,339.855202048648));
#40333=CARTESIAN_POINT('Ctrl Pts',(134.256477538034,0.920222847900195,339.833336453133));
#40334=CARTESIAN_POINT('Ctrl Pts',(134.248725564511,1.05465497763155,339.805798868782));
#40335=CARTESIAN_POINT('Ctrl Pts',(134.240973590988,1.18776908368744,339.772670915361));
#40336=CARTESIAN_POINT('Ctrl Pts',(134.233224900431,1.32082681584048,339.739556991649));
#40337=CARTESIAN_POINT('Ctrl Pts',(134.225476209873,1.45256725599122,339.700857501906));
#40338=CARTESIAN_POINT('Ctrl Pts',(134.217727519316,1.58249181984603,339.656705133742));
#40339=CARTESIAN_POINT('Ctrl Pts',(134.209980440938,1.71238935181019,339.612561951847));
#40340=CARTESIAN_POINT('Ctrl Pts',(134.20223336256,1.84047138910986,339.562968273852));
#40341=CARTESIAN_POINT('Ctrl Pts',(134.194486284182,1.96625503440986,339.508106498538));
#40342=CARTESIAN_POINT('Ctrl Pts',(134.186739140876,2.09203973389788,339.453244263429));
#40343=CARTESIAN_POINT('Ctrl Pts',(134.178991997571,2.21552564468682,339.393113999202));
#40344=CARTESIAN_POINT('Ctrl Pts',(134.171244854265,2.33625073160155,339.327945884781));
#40345=CARTESIAN_POINT('Ctrl Pts',(134.163495969237,2.45700296007889,339.262763119184));
#40346=CARTESIAN_POINT('Ctrl Pts',(134.155747084209,2.57499278568155,339.19254043525));
#40347=CARTESIAN_POINT('Ctrl Pts',(134.147998199181,2.68978397001657,339.117553309569));
#40348=CARTESIAN_POINT('Ctrl Pts',(134.140241089406,2.8046969949007,339.042486591778));
#40349=CARTESIAN_POINT('Ctrl Pts',(134.132483979631,2.91640426878821,338.962645544458));
#40350=CARTESIAN_POINT('Ctrl Pts',(134.124726869856,3.02449924006377,338.8783485415));
#40351=CARTESIAN_POINT('Ctrl Pts',(134.11696561493,3.13265197383574,338.794006492918));
#40352=CARTESIAN_POINT('Ctrl Pts',(134.109204360004,3.23718826095472,338.705203997033));
#40353=CARTESIAN_POINT('Ctrl Pts',(134.101443105078,3.33773648446146,338.61229819129));
#40354=CARTESIAN_POINT('Ctrl Pts',(134.093669434673,3.43844555235721,338.519243766535));
#40355=CARTESIAN_POINT('Ctrl Pts',(134.085895764269,3.53515353243187,338.422073192384));
#40356=CARTESIAN_POINT('Ctrl Pts',(134.078122093864,3.62752676182902,338.321179407186));
#40357=CARTESIAN_POINT('Ctrl Pts',(134.070710289687,3.71559999517437,338.224982251961));
#40358=CARTESIAN_POINT('Ctrl Pts',(134.06329848551,3.79973277541043,338.125400935764));
#40359=CARTESIAN_POINT('Ctrl Pts',(134.055886681333,3.87967238888669,338.022800889475));
#40360=CARTESIAN_POINT('Ctrl Pts',(134.048111602554,3.96353008094701,337.915172109288));
#40361=CARTESIAN_POINT('Ctrl Pts',(134.040336523776,4.04303817972715,337.803881076083));
#40362=CARTESIAN_POINT('Ctrl Pts',(134.032561444997,4.11785985412688,337.689314649547));
#40363=CARTESIAN_POINT('Ctrl Pts',(134.024795933948,4.19258945569285,337.574889204293));
#40364=CARTESIAN_POINT('Ctrl Pts',(134.017030422899,4.2626438957544,337.457196709542));
#40365=CARTESIAN_POINT('Ctrl Pts',(134.00926491185,4.32772657991942,337.336656952135));
#40366=CARTESIAN_POINT('Ctrl Pts',(134.001507100328,4.39274473441363,337.216236710248));
#40367=CARTESIAN_POINT('Ctrl Pts',(133.993749288806,4.45280075850798,337.092975165501));
#40368=CARTESIAN_POINT('Ctrl Pts',(133.985991477284,4.50764157574367,336.967320636583));
#40369=CARTESIAN_POINT('Ctrl Pts',(133.978239503761,4.56244112352525,336.841760666684));
#40370=CARTESIAN_POINT('Ctrl Pts',(133.970487530238,4.61203312046782,336.713811653811));
#40371=CARTESIAN_POINT('Ctrl Pts',(133.962735556715,4.65621079855521,336.583945725686));
#40372=CARTESIAN_POINT('Ctrl Pts',(133.954986866157,4.70036976736972,336.454134795858));
#40373=CARTESIAN_POINT('Ctrl Pts',(133.947238175599,4.73911885225843,336.322408934701));
#40374=CARTESIAN_POINT('Ctrl Pts',(133.939489485042,4.77229982049138,336.18925921726));
#40375=CARTESIAN_POINT('Ctrl Pts',(133.931742406664,4.80547388514676,336.05613720273));
#40376=CARTESIAN_POINT('Ctrl Pts',(133.923995328286,4.8330820430151,335.921592300207));
#40377=CARTESIAN_POINT('Ctrl Pts',(133.916248249908,4.85501635366416,335.786129294807));
#40378=CARTESIAN_POINT('Ctrl Pts',(133.908501106602,4.87695084814386,335.650665154096));
#40379=CARTESIAN_POINT('Ctrl Pts',(133.900753963296,4.89321133808062,335.514283281011));
#40380=CARTESIAN_POINT('Ctrl Pts',(133.893006819991,4.90374135209681,335.377496773808));
#40381=CARTESIAN_POINT('Ctrl Pts',(133.885257934962,4.91427373348371,335.240679514095));
#40382=CARTESIAN_POINT('Ctrl Pts',(133.877509049934,4.9190730453166,335.10345782889));
#40383=CARTESIAN_POINT('Ctrl Pts',(133.869760164906,4.91813486811154,334.966347636554));
#40384=CARTESIAN_POINT('Ctrl Pts',(133.862003055132,4.91719569511549,334.829091914042));
#40385=CARTESIAN_POINT('Ctrl Pts',(133.854245945357,4.91050687075318,334.691948312277));
#40386=CARTESIAN_POINT('Ctrl Pts',(133.846488835582,4.89811611401281,334.555430999565));
#40387=CARTESIAN_POINT('Ctrl Pts',(133.838727580656,4.88571873604822,334.418840736365));
#40388=CARTESIAN_POINT('Ctrl Pts',(133.83096632573,4.86761340599107,334.282877816333));
#40389=CARTESIAN_POINT('Ctrl Pts',(133.823205070804,4.84389934507849,334.148048007662));
#40390=CARTESIAN_POINT('Ctrl Pts',(133.815431400399,4.82014734939685,334.013002515239));
#40391=CARTESIAN_POINT('Ctrl Pts',(133.807657729994,4.79076877767103,333.8790941383));
#40392=CARTESIAN_POINT('Ctrl Pts',(133.799884059589,4.75591349602446,333.746816102548));
#40393=CARTESIAN_POINT('Ctrl Pts',(133.792472255412,4.72268073612439,333.620695641186));
#40394=CARTESIAN_POINT('Ctrl Pts',(133.785060451235,4.68446975778355,333.496057427223));
#40395=CARTESIAN_POINT('Ctrl Pts',(133.777648647058,4.64145110176964,333.373311728578));
#40396=CARTESIAN_POINT('Ctrl Pts',(133.76987356828,4.59632397327837,333.244549897602));
#40397=CARTESIAN_POINT('Ctrl Pts',(133.762098489501,4.54576336359021,333.117463877162));
#40398=CARTESIAN_POINT('Ctrl Pts',(133.754323410723,4.48991231263323,332.99254626769));
#40399=CARTESIAN_POINT('Ctrl Pts',(133.746557899674,4.43412998995011,332.86778237729));
#40400=CARTESIAN_POINT('Ctrl Pts',(133.738792388625,4.37307033749456,332.745181941992));
#40401=CARTESIAN_POINT('Ctrl Pts',(133.731026877576,4.30692585873355,332.625221545097));
#40402=CARTESIAN_POINT('Ctrl Pts',(133.723269066054,4.24084696241581,332.505380089284));
#40403=CARTESIAN_POINT('Ctrl Pts',(133.715511254532,4.16969346041965,332.388173802776));
#40404=CARTESIAN_POINT('Ctrl Pts',(133.70775344301,4.09370539930299,332.274058113932));
#40405=CARTESIAN_POINT('Ctrl Pts',(133.700001469487,4.017774521612,332.160028300764));
#40406=CARTESIAN_POINT('Ctrl Pts',(133.692249495964,3.93701654214815,332.049084779957));
#40407=CARTESIAN_POINT('Ctrl Pts',(133.684497522441,3.8517165891476,331.94165692255));
#40408=CARTESIAN_POINT('Ctrl Pts',(133.676748831883,3.76645276072784,331.834274560905));
#40409=CARTESIAN_POINT('Ctrl Pts',(133.669000141325,3.67665102708774,331.730405206846));
#40410=CARTESIAN_POINT('Ctrl Pts',(133.661251450768,3.58263871490179,331.630447670537));
#40411=CARTESIAN_POINT('Ctrl Pts',(133.65350437239,3.48864596276259,331.530510931229));
#40412=CARTESIAN_POINT('Ctrl Pts',(133.645757294012,3.39044464221962,331.434484675344));
#40413=CARTESIAN_POINT('Ctrl Pts',(133.638010215634,3.28840082508506,331.342732840483));
#40414=CARTESIAN_POINT('Ctrl Pts',(133.630263072328,3.1863561527251,331.250980236654));
#40415=CARTESIAN_POINT('Ctrl Pts',(133.622515929023,3.08046921019923,331.163502386647));
#40416=CARTESIAN_POINT('Ctrl Pts',(133.614768785717,2.97114091287707,331.080624445358));
#40417=CARTESIAN_POINT('Ctrl Pts',(133.607019900689,2.86178803623268,330.997727871348));
#40418=CARTESIAN_POINT('Ctrl Pts',(133.599271015661,2.74899257666471,330.919433499995));
#40419=CARTESIAN_POINT('Ctrl Pts',(133.591522130633,2.6331859892934,330.846024240768));
#40420=CARTESIAN_POINT('Ctrl Pts',(133.583765020858,2.5172564836136,330.772537064194));
#40421=CARTESIAN_POINT('Ctrl Pts',(133.576007911083,2.398309796392,330.703945567087));
#40422=CARTESIAN_POINT('Ctrl Pts',(133.568250801309,2.2768041262092,330.640487867504));
#40423=CARTESIAN_POINT('Ctrl Pts',(133.560489546382,2.15523352728129,330.576996258156));
#40424=CARTESIAN_POINT('Ctrl Pts',(133.552728291456,2.03110157420737,330.518644078881));
#40425=CARTESIAN_POINT('Ctrl Pts',(133.54496703653,1.90488727255615,330.465621592616));
#40426=CARTESIAN_POINT('Ctrl Pts',(133.537193366126,1.77847106915543,330.412514287652));
#40427=CARTESIAN_POINT('Ctrl Pts',(133.529419695721,1.64996622727507,330.364753848958));
#40428=CARTESIAN_POINT('Ctrl Pts',(133.521646025316,1.51986861208891,330.322481163642));
#40429=CARTESIAN_POINT('Ctrl Pts',(133.514234221139,1.39582707218824,330.282176281997));
#40430=CARTESIAN_POINT('Ctrl Pts',(133.506822416962,1.27033798609995,330.246859819564));
#40431=CARTESIAN_POINT('Ctrl Pts',(133.499410612785,1.14383864626459,330.216610384486));
#40432=CARTESIAN_POINT('Ctrl Pts',(133.491635534006,1.01113919696284,330.184878334485));
#40433=CARTESIAN_POINT('Ctrl Pts',(133.483860455228,0.876908604043832,330.158622291981));
#40434=CARTESIAN_POINT('Ctrl Pts',(133.47608537645,0.741638512833184,330.137988546005));
#40435=CARTESIAN_POINT('Ctrl Pts',(133.468319865401,0.606534880081532,330.117380191166));
#40436=CARTESIAN_POINT('Ctrl Pts',(133.460554354352,0.470394676928328,330.102380425216));
#40437=CARTESIAN_POINT('Ctrl Pts',(133.452788843303,0.333722847109352,330.09308527445));
#40438=CARTESIAN_POINT('Ctrl Pts',(133.44503103178,0.197186527807458,330.083799339854));
#40439=CARTESIAN_POINT('Ctrl Pts',(133.437273220258,0.0601200182785917,
330.080206790751));
#40440=CARTESIAN_POINT('Ctrl Pts',(133.429515408736,-0.0769637990857087,
330.082352225288));
#40441=CARTESIAN_POINT('Ctrl Pts',(133.421763435213,-0.213944456530078,
330.084496045318));
#40442=CARTESIAN_POINT('Ctrl Pts',(133.41401146169,-0.350942006632094,330.092369248098));
#40443=CARTESIAN_POINT('Ctrl Pts',(133.406259488167,-0.487441082877129,
330.105964420519));
#40444=CARTESIAN_POINT('Ctrl Pts',(133.398510797609,-0.623882351682428,
330.119553835376));
#40445=CARTESIAN_POINT('Ctrl Pts',(133.390762107052,-0.759825178361284,
330.138860361527));
#40446=CARTESIAN_POINT('Ctrl Pts',(133.383013416494,-0.89475705969261,330.16382456205));
#40447=CARTESIAN_POINT('Ctrl Pts',(133.375266338116,-1.0296608673191,330.188783568563));
#40448=CARTESIAN_POINT('Ctrl Pts',(133.367519259738,-1.16355376386032,330.219397836996));
#40449=CARTESIAN_POINT('Ctrl Pts',(133.359772181361,-1.29593160395851,330.255556477271));
#40450=CARTESIAN_POINT('Ctrl Pts',(133.352025038055,-1.42831055351028,330.291715420591));
#40451=CARTESIAN_POINT('Ctrl Pts',(133.344277894749,-1.55917404423149,330.333418725443));
#40452=CARTESIAN_POINT('Ctrl Pts',(133.336530751443,-1.6880316881225,330.380505213512));
#40453=CARTESIAN_POINT('Ctrl Pts',(133.328781866415,-1.81691830194784,330.427602287622));
#40454=CARTESIAN_POINT('Ctrl Pts',(133.321032981387,-1.9437978045298,330.48008481909));
#40455=CARTESIAN_POINT('Ctrl Pts',(133.313284096359,-2.06819880613954,330.537743086645));
#40456=CARTESIAN_POINT('Ctrl Pts',(133.305526986584,-2.19273184825761,330.595462553282));
#40457=CARTESIAN_POINT('Ctrl Pts',(133.297769876809,-2.31478077912562,330.658368565319));
#40458=CARTESIAN_POINT('Ctrl Pts',(133.290012767035,-2.43389740264501,330.726204673139));
#40459=CARTESIAN_POINT('Ctrl Pts',(133.282251512108,-2.55307767827928,330.794077030407));
#40460=CARTESIAN_POINT('Ctrl Pts',(133.274490257182,-2.66932219321876,330.866884525533));
#40461=CARTESIAN_POINT('Ctrl Pts',(133.266729002256,-2.78221173390346,330.944327314707));
#40462=CARTESIAN_POINT('Ctrl Pts',(133.258955331851,-2.8952818610627,331.021893987106));
#40463=CARTESIAN_POINT('Ctrl Pts',(133.251181661447,-3.00498597643254,331.104110536303));
#40464=CARTESIAN_POINT('Ctrl Pts',(133.243407991042,-3.11093726393982,331.190636220793));
#40465=CARTESIAN_POINT('Ctrl Pts',(133.235996186865,-3.21195649352298,331.273134113854));
#40466=CARTESIAN_POINT('Ctrl Pts',(133.228584382688,-3.30956420526994,331.359548799256));
#40467=CARTESIAN_POINT('Ctrl Pts',(133.221172578511,-3.40345765188556,331.449555087835));
#40468=CARTESIAN_POINT('Ctrl Pts',(133.213511082815,-3.5005142146269,331.542593540564));
#40469=CARTESIAN_POINT('Ctrl Pts',(133.205849587119,-3.59392796942943,331.639782791326));
#40470=CARTESIAN_POINT('Ctrl Pts',(133.198188091422,-3.6833150462342,331.740801734677));
#40471=CARTESIAN_POINT('Ctrl Pts',(133.190536156553,-3.77259057636755,331.84169461588));
#40472=CARTESIAN_POINT('Ctrl Pts',(133.182884221683,-3.85784915697961,331.946407386533));
#40473=CARTESIAN_POINT('Ctrl Pts',(133.175232286814,-3.93874150010774,332.05458008803));
#40474=CARTESIAN_POINT('Ctrl Pts',(133.167589038231,-4.01954201625486,332.16262999456));
#40475=CARTESIAN_POINT('Ctrl Pts',(133.159945789648,-4.09598592049617,332.274131693386));
#40476=CARTESIAN_POINT('Ctrl Pts',(133.152302541065,-4.16776268013728,332.388690500045));
#40477=CARTESIAN_POINT('Ctrl Pts',(133.144664156999,-4.23949375773086,332.503176396185));
#40478=CARTESIAN_POINT('Ctrl Pts',(133.137025772933,-4.30656338277509,332.620715191685));
#40479=CARTESIAN_POINT('Ctrl Pts',(133.129387388867,-4.36870312452959,332.74088157189));
#40480=CARTESIAN_POINT('Ctrl Pts',(133.121752099894,-4.43081768709791,332.860999260363));
#40481=CARTESIAN_POINT('Ctrl Pts',(133.114116810921,-4.48800615405122,332.983742058596));
#40482=CARTESIAN_POINT('Ctrl Pts',(133.106481521948,-4.54004531548502,333.108658783867));
#40483=CARTESIAN_POINT('Ctrl Pts',(133.098847561528,-4.592075422017,333.233553773417));
#40484=CARTESIAN_POINT('Ctrl Pts',(133.091213601108,-4.63895785133504,333.360621565049));
#40485=CARTESIAN_POINT('Ctrl Pts',(133.083579640688,-4.68051717966776,333.489390191567));
#40486=CARTESIAN_POINT('Ctrl Pts',(133.075942212416,-4.7220953870101,333.618217313355));
#40487=CARTESIAN_POINT('Ctrl Pts',(133.068304784144,-4.75834553472749,333.748746430563));
#40488=CARTESIAN_POINT('Ctrl Pts',(133.060667355872,-4.78914182396789,333.880489547873));
#40489=CARTESIAN_POINT('Ctrl Pts',(133.053028265726,-4.81994481435949,334.012261331966));
#40490=CARTESIAN_POINT('Ctrl Pts',(133.04538917558,-4.84529150255409,334.145247246808));
#40491=CARTESIAN_POINT('Ctrl Pts',(133.037750085433,-4.86510731614558,334.278949471336));
#40492=CARTESIAN_POINT('Ctrl Pts',(133.030103040723,-4.88494376388924,334.412790919622));
#40493=CARTESIAN_POINT('Ctrl Pts',(133.022455996013,-4.89923778582828,334.547349766649));
#40494=CARTESIAN_POINT('Ctrl Pts',(133.014808951304,-4.90796672328694,334.682123128227));
#40495=CARTESIAN_POINT('Ctrl Pts',(133.008718050377,-4.91491935600626,334.789470636196));
#40496=CARTESIAN_POINT('Ctrl Pts',(133.00262714945,-4.91834241697973,334.896954093159));
#40497=CARTESIAN_POINT('Ctrl Pts',(132.996536248523,-4.91824810241123,335.004320373636));
#40498=CARTESIAN_POINT('',(136.49653624846,-4.91824792654204,334.995483855083));
#40499=CARTESIAN_POINT('Ctrl Pts',(136.49653624846,-4.91824792654204,334.995483855083));
#40500=CARTESIAN_POINT('Ctrl Pts',(136.488880220191,-4.91837200760644,335.130612698127));
#40501=CARTESIAN_POINT('Ctrl Pts',(136.481224191922,-4.91292290562032,335.265902532329));
#40502=CARTESIAN_POINT('Ctrl Pts',(136.473568163653,-4.9018876379854,335.400849905907));
#40503=CARTESIAN_POINT('Ctrl Pts',(136.465577446647,-4.89036995575505,335.541696600172));
#40504=CARTESIAN_POINT('Ctrl Pts',(136.457586729642,-4.87276658776302,335.682169772044));
#40505=CARTESIAN_POINT('Ctrl Pts',(136.449596012637,-4.84912339044322,335.821696663469));
#40506=CARTESIAN_POINT('Ctrl Pts',(136.441948571372,-4.82649588872065,335.955229575002));
#40507=CARTESIAN_POINT('Ctrl Pts',(136.434301130108,-4.79833678172102,336.087895379985));
#40508=CARTESIAN_POINT('Ctrl Pts',(136.426653688844,-4.76473917465448,336.219197957681));
#40509=CARTESIAN_POINT('Ctrl Pts',(136.419007402992,-4.73114664367949,336.350480697538));
#40510=CARTESIAN_POINT('Ctrl Pts',(136.411361117141,-4.69211734596046,336.480400230189));
#40511=CARTESIAN_POINT('Ctrl Pts',(136.40371483129,-4.64779509938816,336.608472497932));
#40512=CARTESIAN_POINT('Ctrl Pts',(136.396067943003,-4.60346936075534,336.736554856231));
#40513=CARTESIAN_POINT('Ctrl Pts',(136.388421054716,-4.55384997580059,336.862789280302));
#40514=CARTESIAN_POINT('Ctrl Pts',(136.380774166429,-4.49912986394917,336.986709221255));
#40515=CARTESIAN_POINT('Ctrl Pts',(136.373124917608,-4.44439286042653,337.110667415327));
#40516=CARTESIAN_POINT('Ctrl Pts',(136.365475668787,-4.38455216153253,337.232309338066));
#40517=CARTESIAN_POINT('Ctrl Pts',(136.357826419965,-4.31984757795824,337.35119118017));
#40518=CARTESIAN_POINT('Ctrl Pts',(136.350168933632,-4.25507331371344,337.470201046688));
#40519=CARTESIAN_POINT('Ctrl Pts',(136.342511447298,-4.18542490274012,337.586444546877));
#40520=CARTESIAN_POINT('Ctrl Pts',(136.334853960964,-4.1111867358577,337.699504896348));
#40521=CARTESIAN_POINT('Ctrl Pts',(136.327191619778,-4.03690150191032,337.812636926184));
#40522=CARTESIAN_POINT('Ctrl Pts',(136.319529278591,-3.95802095341253,337.922581462587));
#40523=CARTESIAN_POINT('Ctrl Pts',(136.311866937404,-3.87487022793623,338.028954238537));
#40524=CARTESIAN_POINT('Ctrl Pts',(136.304193797532,-3.79160231653885,338.135476927692));
#40525=CARTESIAN_POINT('Ctrl Pts',(136.29652065766,-3.70405247838207,338.238417506861));
#40526=CARTESIAN_POINT('Ctrl Pts',(136.288847517788,-3.6125833477282,338.337427844646));
#40527=CARTESIAN_POINT('Ctrl Pts',(136.286495330367,-3.58454364792289,338.367779288125));
#40528=CARTESIAN_POINT('Ctrl Pts',(136.284143142945,-3.55613588360524,338.397761682906));
#40529=CARTESIAN_POINT('Ctrl Pts',(136.281790955524,-3.52737111106981,338.427365767946));
#40530=CARTESIAN_POINT('Ctrl Pts',(136.274015876745,-3.43229009394204,338.525221105175));
#40531=CARTESIAN_POINT('Ctrl Pts',(136.266240797967,-3.33298373222669,338.619271508503));
#40532=CARTESIAN_POINT('Ctrl Pts',(136.258465719188,-3.22978891642843,338.709130169975));
#40533=CARTESIAN_POINT('Ctrl Pts',(136.250700208139,-3.12672108842059,338.798878254643));
#40534=CARTESIAN_POINT('Ctrl Pts',(136.24293469709,-3.01977461905091,338.884444606572));
#40535=CARTESIAN_POINT('Ctrl Pts',(136.235169186041,-2.90932454398892,338.965477746785));
#40536=CARTESIAN_POINT('Ctrl Pts',(136.227411374519,-2.79898398049803,339.046430542402));
#40537=CARTESIAN_POINT('Ctrl Pts',(136.219653562997,-2.68514703756664,339.122858841268));
#40538=CARTESIAN_POINT('Ctrl Pts',(136.211895751475,-2.56822299344343,339.194450347596));
#40539=CARTESIAN_POINT('Ctrl Pts',(136.204143777952,-2.45138693837106,339.265987979046));
#40540=CARTESIAN_POINT('Ctrl Pts',(136.196391804429,-2.33146873821512,339.332695859595));
#40541=CARTESIAN_POINT('Ctrl Pts',(136.188639830906,-2.20890761936723,339.394304289828));
#40542=CARTESIAN_POINT('Ctrl Pts',(136.180891140348,-2.08639840522611,339.455886628854));
#40543=CARTESIAN_POINT('Ctrl Pts',(136.173142449791,-1.96124884706467,339.512373637709));
#40544=CARTESIAN_POINT('Ctrl Pts',(136.165393759233,-1.83392360993417,339.563541087295));
#40545=CARTESIAN_POINT('Ctrl Pts',(136.157646680855,-1.70662486388266,339.614697891065));
#40546=CARTESIAN_POINT('Ctrl Pts',(136.149899602477,-1.57715170170746,339.660537191367));
#40547=CARTESIAN_POINT('Ctrl Pts',(136.142152524099,-1.4459892810726,339.700882689615));
#40548=CARTESIAN_POINT('Ctrl Pts',(136.134405380794,-1.31482576117042,339.741228525997));
#40549=CARTESIAN_POINT('Ctrl Pts',(136.126658237488,-1.18197332816933,339.776080353569));
#40550=CARTESIAN_POINT('Ctrl Pts',(136.118911094182,-1.04793244838807,339.805311711649));
#40551=CARTESIAN_POINT('Ctrl Pts',(136.111162209154,-0.913861433370988,
339.83454964156));
#40552=CARTESIAN_POINT('Ctrl Pts',(136.103413324126,-0.778601821723289,
339.858164504288));
#40553=CARTESIAN_POINT('Ctrl Pts',(136.095664439098,-0.642664027625574,
339.876081009386));
#40554=CARTESIAN_POINT('Ctrl Pts',(136.087907329323,-0.50658194774898,339.894016531247));
#40555=CARTESIAN_POINT('Ctrl Pts',(136.080150219548,-0.369820635629727,
339.906241562284));
#40556=CARTESIAN_POINT('Ctrl Pts',(136.072393109773,-0.232895938429691,
339.912732696205));
#40557=CARTESIAN_POINT('Ctrl Pts',(136.064631854847,-0.0958980730494751,
339.91922729878));
#40558=CARTESIAN_POINT('Ctrl Pts',(136.056870599921,0.0412629607100064,
339.919981896772));
#40559=CARTESIAN_POINT('Ctrl Pts',(136.049109344995,0.178072557094469,339.91502525191));
#40560=CARTESIAN_POINT('Ctrl Pts',(136.04133567459,0.31510100424691,339.910060678031));
#40561=CARTESIAN_POINT('Ctrl Pts',(136.033562004186,0.451776500723456,339.899366635117));
#40562=CARTESIAN_POINT('Ctrl Pts',(136.025788333781,0.587589903084384,339.883023773062));
#40563=CARTESIAN_POINT('Ctrl Pts',(136.018376529604,0.717081158889626,339.867441675169));
#40564=CARTESIAN_POINT('Ctrl Pts',(136.010964725427,0.845788491179478,339.846724873767));
#40565=CARTESIAN_POINT('Ctrl Pts',(136.00355292125,0.973282085195013,339.820985899703));
#40566=CARTESIAN_POINT('Ctrl Pts',(135.995777842472,1.10702452003798,339.793985381848));
#40567=CARTESIAN_POINT('Ctrl Pts',(135.988002763693,1.23985388119609,339.761372613526));
#40568=CARTESIAN_POINT('Ctrl Pts',(135.980227684915,1.37126258282383,339.723221569167));
#40569=CARTESIAN_POINT('Ctrl Pts',(135.972462173866,1.50250957767816,339.685117472098));
#40570=CARTESIAN_POINT('Ctrl Pts',(135.964696662817,1.63233901965662,339.641488767228));
#40571=CARTESIAN_POINT('Ctrl Pts',(135.956931151768,1.76025238926696,339.592460624609));
#40572=CARTESIAN_POINT('Ctrl Pts',(135.949173340245,1.88803893239909,339.543481093536));
#40573=CARTESIAN_POINT('Ctrl Pts',(135.941415528723,2.01391282122397,339.489112917591));
#40574=CARTESIAN_POINT('Ctrl Pts',(135.933657717201,2.13738995560857,339.429531266417));
#40575=CARTESIAN_POINT('Ctrl Pts',(135.925905743678,2.26077416953356,339.369994452325));
#40576=CARTESIAN_POINT('Ctrl Pts',(135.918153770155,2.38176486844677,339.305252141334));
#40577=CARTESIAN_POINT('Ctrl Pts',(135.910401796632,2.49989756575133,339.235527738458));
#40578=CARTESIAN_POINT('Ctrl Pts',(135.902653106075,2.61798023378877,339.165832863909));
#40579=CARTESIAN_POINT('Ctrl Pts',(135.894904415517,2.73320697163412,339.091160292218));
#40580=CARTESIAN_POINT('Ctrl Pts',(135.887155724959,2.84513776333188,339.011779426908));
#40581=CARTESIAN_POINT('Ctrl Pts',(135.879408646581,2.95704526689345,338.932415077451));
#40582=CARTESIAN_POINT('Ctrl Pts',(135.871661568204,3.06565786967789,338.848344608841));
#40583=CARTESIAN_POINT('Ctrl Pts',(135.863914489826,3.17056477179156,338.759880595228));
#40584=CARTESIAN_POINT('Ctrl Pts',(135.85616734652,3.2754725531259,338.671415840202));
#40585=CARTESIAN_POINT('Ctrl Pts',(135.848420203214,3.37667427302956,338.578557718706));
#40586=CARTESIAN_POINT('Ctrl Pts',(135.840673059908,3.47379275697694,338.481658648414));
#40587=CARTESIAN_POINT('Ctrl Pts',(135.83292417488,3.57093307522166,338.384737793153));
#40588=CARTESIAN_POINT('Ctrl Pts',(135.825175289852,3.66398805414817,338.283774457325));
#40589=CARTESIAN_POINT('Ctrl Pts',(135.817426404824,3.75261816601189,338.17915711512));
#40590=CARTESIAN_POINT('Ctrl Pts',(135.809669295049,3.84134235079202,338.074428730987));
#40591=CARTESIAN_POINT('Ctrl Pts',(135.801912185275,3.92563203355077,337.966038891718));
#40592=CARTESIAN_POINT('Ctrl Pts',(135.7941550755,4.00518837693964,337.854408717708));
#40593=CARTESIAN_POINT('Ctrl Pts',(135.786393820574,4.08478723269454,337.742718892103));
#40594=CARTESIAN_POINT('Ctrl Pts',(135.778632565648,4.15964749591002,337.627785608884));
#40595=CARTESIAN_POINT('Ctrl Pts',(135.770871310722,4.22951487023652,337.510057175633));
#40596=CARTESIAN_POINT('Ctrl Pts',(135.763097640317,4.29949400959234,337.392140415256));
#40597=CARTESIAN_POINT('Ctrl Pts',(135.755323969912,4.36446411434039,337.271419914181));
#40598=CARTESIAN_POINT('Ctrl Pts',(135.747550299508,4.42421747796838,337.148367466273));
#40599=CARTESIAN_POINT('Ctrl Pts',(135.74013849533,4.48118930814455,337.031043139418));
#40600=CARTESIAN_POINT('Ctrl Pts',(135.732726691153,4.53341903060046,336.911599347874));
#40601=CARTESIAN_POINT('Ctrl Pts',(135.725314886976,4.58076867749739,336.790458428939));
#40602=CARTESIAN_POINT('Ctrl Pts',(135.717539808198,4.63043907163535,336.663380032709));
#40603=CARTESIAN_POINT('Ctrl Pts',(135.709764729419,4.67489588805964,336.534032348861));
#40604=CARTESIAN_POINT('Ctrl Pts',(135.701989650641,4.7139266496224,336.402882248972));
#40605=CARTESIAN_POINT('Ctrl Pts',(135.694224139592,4.75290938134819,336.27189353763));
#40606=CARTESIAN_POINT('Ctrl Pts',(135.686458628543,4.78647923331155,336.13910719446));
#40607=CARTESIAN_POINT('Ctrl Pts',(135.678693117494,4.81447168617738,336.005010171837));
#40608=CARTESIAN_POINT('Ctrl Pts',(135.670935305971,4.84243638444472,335.871046106802));
#40609=CARTESIAN_POINT('Ctrl Pts',(135.663177494449,4.8648346092841,335.735774328639));
#40610=CARTESIAN_POINT('Ctrl Pts',(135.655419682927,4.88155169022486,335.599696721821));
#40611=CARTESIAN_POINT('Ctrl Pts',(135.647667709404,4.89825619103208,335.463721517717));
#40612=CARTESIAN_POINT('Ctrl Pts',(135.639915735881,4.90928801013023,335.326942078388));
#40613=CARTESIAN_POINT('Ctrl Pts',(135.632163762358,4.91458365321138,335.189869897792));
#40614=CARTESIAN_POINT('Ctrl Pts',(135.6244150718,4.91987705358453,335.052855767346));
#40615=CARTESIAN_POINT('Ctrl Pts',(135.616666381243,4.91943909453702,334.915549531984));
#40616=CARTESIAN_POINT('Ctrl Pts',(135.608917690685,4.91325820535681,334.778467000214));
#40617=CARTESIAN_POINT('Ctrl Pts',(135.601170612307,4.90707860216221,334.641412989611));
#40618=CARTESIAN_POINT('Ctrl Pts',(135.593423533929,4.89515846310018,334.504582980254));
#40619=CARTESIAN_POINT('Ctrl Pts',(135.585676455552,4.87753833104645,334.368491574346));
#40620=CARTESIAN_POINT('Ctrl Pts',(135.577929312246,4.85991805131904,334.23239902786));
#40621=CARTESIAN_POINT('Ctrl Pts',(135.57018216894,4.83659773350489,334.097045484809));
#40622=CARTESIAN_POINT('Ctrl Pts',(135.562435025634,4.80766962236658,333.962938832723));
#40623=CARTESIAN_POINT('Ctrl Pts',(135.554686140606,4.77873500757465,333.828802030614));
#40624=CARTESIAN_POINT('Ctrl Pts',(135.546937255578,4.74419017310846,333.695913059302));
#40625=CARTESIAN_POINT('Ctrl Pts',(135.53918837055,4.70417805725921,333.564767660586));
#40626=CARTESIAN_POINT('Ctrl Pts',(135.531431260775,4.66412347213697,333.433483062789));
#40627=CARTESIAN_POINT('Ctrl Pts',(135.523674151,4.61859012778119,333.303946108879));
#40628=CARTESIAN_POINT('Ctrl Pts',(135.515917041226,4.56777043528063,333.176635989969));
#40629=CARTESIAN_POINT('Ctrl Pts',(135.5081557863,4.51692358636127,333.049257840602));
#40630=CARTESIAN_POINT('Ctrl Pts',(135.500394531373,4.46078492041568,332.92410925377));
#40631=CARTESIAN_POINT('Ctrl Pts',(135.492633276447,4.39959381450564,332.801646677655));
#40632=CARTESIAN_POINT('Ctrl Pts',(135.484859606043,4.33830482276827,332.678988201329));
#40633=CARTESIAN_POINT('Ctrl Pts',(135.477085935638,4.27194742961757,332.559024664097));
#40634=CARTESIAN_POINT('Ctrl Pts',(135.469312265233,4.20080597466927,332.44218604553));
#40635=CARTESIAN_POINT('Ctrl Pts',(135.461900461056,4.13297617156452,332.330786292766));
#40636=CARTESIAN_POINT('Ctrl Pts',(135.454488656879,4.06079783879632,332.222227315595));
#40637=CARTESIAN_POINT('Ctrl Pts',(135.447076852702,3.98455146649534,332.11685368506));
#40638=CARTESIAN_POINT('Ctrl Pts',(135.439301773924,3.90456803236149,332.006315379001));
#40639=CARTESIAN_POINT('Ctrl Pts',(135.431526695145,3.81985493980073,331.898933239927));
#40640=CARTESIAN_POINT('Ctrl Pts',(135.423751616367,3.73068980750526,331.795138595403));
#40641=CARTESIAN_POINT('Ctrl Pts',(135.415986105318,3.64163439858168,331.691471676797));
#40642=CARTESIAN_POINT('Ctrl Pts',(135.408220594269,3.54813810287312,331.591383762532));
#40643=CARTESIAN_POINT('Ctrl Pts',(135.40045508322,3.45052137816715,331.495276718297));
#40644=CARTESIAN_POINT('Ctrl Pts',(135.392697271697,3.35300144072778,331.399264964476));
#40645=CARTESIAN_POINT('Ctrl Pts',(135.384939460175,3.25136948124354,331.307226498306));
#40646=CARTESIAN_POINT('Ctrl Pts',(135.377181648653,3.14598549030458,331.219529347119));
#40647=CARTESIAN_POINT('Ctrl Pts',(135.36942967513,3.04068080416094,331.13189819082));
#40648=CARTESIAN_POINT('Ctrl Pts',(135.361677701607,2.93163000588674,331.048602095762));
#40649=CARTESIAN_POINT('Ctrl Pts',(135.353925728084,2.81922886125216,330.969971254397));
#40650=CARTESIAN_POINT('Ctrl Pts',(135.346177037526,2.70687531856899,330.891373713241));
#40651=CARTESIAN_POINT('Ctrl Pts',(135.338428346969,2.5911745711822,330.817437719762));
#40652=CARTESIAN_POINT('Ctrl Pts',(135.330679656411,2.47255411189487,330.748452137603));
#40653=CARTESIAN_POINT('Ctrl Pts',(135.322932578033,2.35395833258491,330.67948090847));
#40654=CARTESIAN_POINT('Ctrl Pts',(135.315185499655,2.2324443873526,330.615458238345));
#40655=CARTESIAN_POINT('Ctrl Pts',(135.307438421278,2.10846695624441,330.556628514638));
#40656=CARTESIAN_POINT('Ctrl Pts',(135.299691277972,1.98448848608576,330.497798297881));
#40657=CARTESIAN_POINT('Ctrl Pts',(135.291944134666,1.85804684200413,330.444161281919));
#40658=CARTESIAN_POINT('Ctrl Pts',(135.28419699136,1.72961903639317,330.395914743247));
#40659=CARTESIAN_POINT('Ctrl Pts',(135.276448106332,1.60116235748504,330.34765735773));
#40660=CARTESIAN_POINT('Ctrl Pts',(135.268699221304,1.47071899433501,330.30479299847));
#40661=CARTESIAN_POINT('Ctrl Pts',(135.260950336276,1.33878317890999,330.267469739942));
#40662=CARTESIAN_POINT('Ctrl Pts',(135.253193226501,1.20670732544751,330.230106866122));
#40663=CARTESIAN_POINT('Ctrl Pts',(135.245436116726,1.07313623202158,330.198296948212));
#40664=CARTESIAN_POINT('Ctrl Pts',(135.237679006952,0.938576985342084,330.172137501431));
#40665=CARTESIAN_POINT('Ctrl Pts',(135.229917752026,0.803945834503438,330.145964075878));
#40666=CARTESIAN_POINT('Ctrl Pts',(135.222156497099,0.668325864529675,330.125447196379));
#40667=CARTESIAN_POINT('Ctrl Pts',(135.214395242173,0.532230453097473,330.110632575957));
#40668=CARTESIAN_POINT('Ctrl Pts',(135.206621571769,0.395917333360418,330.09579425697));
#40669=CARTESIAN_POINT('Ctrl Pts',(135.198847901364,0.259127642572011,330.086676451041));
#40670=CARTESIAN_POINT('Ctrl Pts',(135.191074230959,0.122376832207485,330.083272737538));
#40671=CARTESIAN_POINT('Ctrl Pts',(135.183662426782,-0.00800819503385429,
330.080027467717));
#40672=CARTESIAN_POINT('Ctrl Pts',(135.176250622605,-0.138357592394053,
330.081976275939));
#40673=CARTESIAN_POINT('Ctrl Pts',(135.168838818428,-0.268229813425918,
330.089069759232));
#40674=CARTESIAN_POINT('Ctrl Pts',(135.16106373965,-0.404467458880331,330.096510915272));
#40675=CARTESIAN_POINT('Ctrl Pts',(135.153288660871,-0.540610505746174,
330.109637325042));
#40676=CARTESIAN_POINT('Ctrl Pts',(135.145513582093,-0.676146006067357,
330.128448949156));
#40677=CARTESIAN_POINT('Ctrl Pts',(135.137748071044,-0.811514721326461,
330.147237424369));
#40678=CARTESIAN_POINT('Ctrl Pts',(135.129982559995,-0.94627699413789,330.171697140634));
#40679=CARTESIAN_POINT('Ctrl Pts',(135.122217048946,-1.07992146897312,330.201776090745));
#40680=CARTESIAN_POINT('Ctrl Pts',(135.114459237424,-1.21343343492265,330.231825217488));
#40681=CARTESIAN_POINT('Ctrl Pts',(135.106701425902,-1.34582942959668,330.26748240523));
#40682=CARTESIAN_POINT('Ctrl Pts',(135.098943614379,-1.47660515939545,330.308644090911));
#40683=CARTESIAN_POINT('Ctrl Pts',(135.091191640856,-1.6072824763105,330.349774801117));
#40684=CARTESIAN_POINT('Ctrl Pts',(135.083439667333,-1.73634158396792,330.396401647318));
#40685=CARTESIAN_POINT('Ctrl Pts',(135.07568769381,-1.86329064492519,330.448370507715));
#40686=CARTESIAN_POINT('Ctrl Pts',(135.067939003253,-1.99018594287999,330.500317359269));
#40687=CARTESIAN_POINT('Ctrl Pts',(135.060190312695,-2.11497261046951,330.557601577597));
#40688=CARTESIAN_POINT('Ctrl Pts',(135.052441622138,-2.23717639521115,330.62001999557));
#40689=CARTESIAN_POINT('Ctrl Pts',(135.04469454376,-2.35935475443446,330.682425426869));
#40690=CARTESIAN_POINT('Ctrl Pts',(135.036947465382,-2.47895095184019,330.749962755377));
#40691=CARTESIAN_POINT('Ctrl Pts',(135.029200387004,-2.59551342337868,330.822381882991));
#40692=CARTESIAN_POINT('Ctrl Pts',(135.021453243698,-2.71207687182351,330.894801617548));
#40693=CARTESIAN_POINT('Ctrl Pts',(135.013706100392,-2.8256062116748,330.972103026542));
#40694=CARTESIAN_POINT('Ctrl Pts',(135.005958957087,-2.9356774101408,331.053991737706));
#40695=CARTESIAN_POINT('Ctrl Pts',(134.998210072058,-3.04577335494865,331.135898859191));
#40696=CARTESIAN_POINT('Ctrl Pts',(134.99046118703,-3.15240929776071,331.222395101799));
#40697=CARTESIAN_POINT('Ctrl Pts',(134.982712302002,-3.25519326231551,331.31314498692));
#40698=CARTESIAN_POINT('Ctrl Pts',(134.974955192228,-3.35808632283232,331.403991194906));
#40699=CARTESIAN_POINT('Ctrl Pts',(134.967198082453,-3.4571189443977,331.499099805149));
#40700=CARTESIAN_POINT('Ctrl Pts',(134.959440972678,-3.55193471066977,331.598097168695));
#40701=CARTESIAN_POINT('Ctrl Pts',(134.951679717752,-3.64680114345565,331.697147433267));
#40702=CARTESIAN_POINT('Ctrl Pts',(134.943918462826,-3.73744597276019,331.800090298588));
#40703=CARTESIAN_POINT('Ctrl Pts',(134.9361572079,-3.82355293940824,331.906518792357));
#40704=CARTESIAN_POINT('Ctrl Pts',(134.928383537495,-3.90979764914072,332.01311753703));
#40705=CARTESIAN_POINT('Ctrl Pts',(134.92060986709,-3.99148975734294,332.123212738326));
#40706=CARTESIAN_POINT('Ctrl Pts',(134.912836196686,-4.0683557228909,332.236367467531));
#40707=CARTESIAN_POINT('Ctrl Pts',(134.905424392509,-4.1416435592496,332.344254816868));
#40708=CARTESIAN_POINT('Ctrl Pts',(134.898012588332,-4.21054430319857,332.454923017942));
#40709=CARTESIAN_POINT('Ctrl Pts',(134.890600784154,-4.2748605526315,332.567974030144));
#40710=CARTESIAN_POINT('Ctrl Pts',(134.882487617091,-4.34526290867109,332.691722813412));
#40711=CARTESIAN_POINT('Ctrl Pts',(134.874374450027,-4.41037836836449,332.81868940777));
#40712=CARTESIAN_POINT('Ctrl Pts',(134.866261282963,-4.46991427174387,332.948403191229));
#40713=CARTESIAN_POINT('Ctrl Pts',(134.858161266845,-4.52935367107875,333.077906716607));
#40714=CARTESIAN_POINT('Ctrl Pts',(134.850061250727,-4.58323139045913,333.210148250226));
#40715=CARTESIAN_POINT('Ctrl Pts',(134.841961234609,-4.63129969921503,333.344631111036));
#40716=CARTESIAN_POINT('Ctrl Pts',(134.833878080244,-4.67926794447111,333.478834019709));
#40717=CARTESIAN_POINT('Ctrl Pts',(134.825794925879,-4.7214507781199,333.615268631362));
#40718=CARTESIAN_POINT('Ctrl Pts',(134.817711771514,-4.7576480650366,333.753417490997));
#40719=CARTESIAN_POINT('Ctrl Pts',(134.809638480598,-4.79380118230602,333.891397774836));
#40720=CARTESIAN_POINT('Ctrl Pts',(134.801565189681,-4.82398321470201,334.031087810636));
#40721=CARTESIAN_POINT('Ctrl Pts',(134.793491898765,-4.84804299991267,334.17195281928));
#40722=CARTESIAN_POINT('Ctrl Pts',(134.785431051445,-4.87206570108183,334.31260070862));
#40723=CARTESIAN_POINT('Ctrl Pts',(134.777370204125,-4.88998491290346,334.454419623487));
#40724=CARTESIAN_POINT('Ctrl Pts',(134.769309356805,-4.90170006679297,334.596862904582));
#40725=CARTESIAN_POINT('Ctrl Pts',(134.7617183207,-4.91273242513222,334.731004148896));
#40726=CARTESIAN_POINT('Ctrl Pts',(134.754127284595,-4.91826319865876,334.865698748933));
#40727=CARTESIAN_POINT('Ctrl Pts',(134.74653624849,-4.9182499763342,335.000482481796));
#40728=CARTESIAN_POINT('',(138.246536248522,-4.91824966475132,335.001815949749));
#40729=CARTESIAN_POINT('Ctrl Pts',(138.24653624849,-4.91824966475112,335.001815950303));
#40730=CARTESIAN_POINT('Ctrl Pts',(138.240843230807,-4.91821275526505,335.101780176863));
#40731=CARTESIAN_POINT('Ctrl Pts',(138.235150213124,-4.91512839652291,335.201684563828));
#40732=CARTESIAN_POINT('Ctrl Pts',(138.229457195442,-4.90900608956926,335.30140052268));
#40733=CARTESIAN_POINT('Ctrl Pts',(138.221682116663,-4.90064472104323,335.437584788873));
#40734=CARTESIAN_POINT('Ctrl Pts',(138.213907037885,-4.88659886760582,335.5736360507));
#40735=CARTESIAN_POINT('Ctrl Pts',(138.206131959106,-4.86687203397043,335.709041372176));
#40736=CARTESIAN_POINT('Ctrl Pts',(138.198366448057,-4.8471694754597,335.844280068783));
#40737=CARTESIAN_POINT('Ctrl Pts',(138.190600937008,-4.82179990226589,335.97887402351));
#40738=CARTESIAN_POINT('Ctrl Pts',(138.182835425959,-4.7908187749794,336.112312243844));
#40739=CARTESIAN_POINT('Ctrl Pts',(138.175077614437,-4.75986836557079,336.245618159794));
#40740=CARTESIAN_POINT('Ctrl Pts',(138.167319802915,-4.72331756232056,336.37777024349));
#40741=CARTESIAN_POINT('Ctrl Pts',(138.159561991393,-4.68127333278809,336.508264912483));
#40742=CARTESIAN_POINT('Ctrl Pts',(138.15181001787,-4.63926074287154,336.638661380099));
#40743=CARTESIAN_POINT('Ctrl Pts',(138.144058044347,-4.59176307453842,336.767402545074));
#40744=CARTESIAN_POINT('Ctrl Pts',(138.136306070824,-4.53893776878225,336.893997622391));
#40745=CARTESIAN_POINT('Ctrl Pts',(138.128557380266,-4.48613483457457,337.020539086617));
#40746=CARTESIAN_POINT('Ctrl Pts',(138.120808689709,-4.42800890069209,337.144935910884));
#40747=CARTESIAN_POINT('Ctrl Pts',(138.113059999151,-4.3647663335395,337.266715226071));
#40748=CARTESIAN_POINT('Ctrl Pts',(138.105312920773,-4.3015369245312,337.388469204054));
#40749=CARTESIAN_POINT('Ctrl Pts',(138.097565842395,-4.23319317976694,337.507606409525));
#40750=CARTESIAN_POINT('Ctrl Pts',(138.089818764018,-4.1599882422768,337.62367697833));
#40751=CARTESIAN_POINT('Ctrl Pts',(138.082071620712,-4.08678269125879,337.739748519918));
#40752=CARTESIAN_POINT('Ctrl Pts',(138.074324477406,-4.00871607476777,337.852753042965));
#40753=CARTESIAN_POINT('Ctrl Pts',(138.0665773341,-3.92608562299602,337.962268513049));
#40754=CARTESIAN_POINT('Ctrl Pts',(138.058828449072,-3.8434365941445,338.071808604536));
#40755=CARTESIAN_POINT('Ctrl Pts',(138.051079564044,-3.75622192367133,338.177857770205));
#40756=CARTESIAN_POINT('Ctrl Pts',(138.043330679016,-3.66477973060957,338.280026309134));
#40757=CARTESIAN_POINT('Ctrl Pts',(138.035573569241,-3.57324047985925,338.382303290807));
#40758=CARTESIAN_POINT('Ctrl Pts',(138.027816459466,-3.47746500413433,338.480691126062));
#40759=CARTESIAN_POINT('Ctrl Pts',(138.020059349692,-3.37782935170732,338.574835930955));
#40760=CARTESIAN_POINT('Ctrl Pts',(138.012298094765,-3.27814045717343,338.669031043821));
#40761=CARTESIAN_POINT('Ctrl Pts',(138.004536839839,-3.1745875706577,338.758978352254));
#40762=CARTESIAN_POINT('Ctrl Pts',(137.996775584913,-3.06757979172964,338.844364353683));
#40763=CARTESIAN_POINT('Ctrl Pts',(137.989001914508,-2.96040083522901,338.929886944888));
#40764=CARTESIAN_POINT('Ctrl Pts',(137.981228244104,-2.84975625795989,339.010833417398));
#40765=CARTESIAN_POINT('Ctrl Pts',(137.973454573699,-2.7360848266308,339.086933188098));
#40766=CARTESIAN_POINT('Ctrl Pts',(137.966042769522,-2.62770482777796,339.159490496164));
#40767=CARTESIAN_POINT('Ctrl Pts',(137.958630965345,-2.51657367857949,339.2276420253));
#40768=CARTESIAN_POINT('Ctrl Pts',(137.951219161168,-2.40309074415355,339.291193066953));
#40769=CARTESIAN_POINT('Ctrl Pts',(137.943444082389,-2.2840456730631,339.357858934466));
#40770=CARTESIAN_POINT('Ctrl Pts',(137.935669003611,-2.16203624722082,339.419672621049));
#40771=CARTESIAN_POINT('Ctrl Pts',(137.927893924833,-2.03749570204059,339.476359494798));
#40772=CARTESIAN_POINT('Ctrl Pts',(137.920128413784,-1.91310841192979,339.532976611739));
#40773=CARTESIAN_POINT('Ctrl Pts',(137.912362902735,-1.78619655220239,339.584479308307));
#40774=CARTESIAN_POINT('Ctrl Pts',(137.904597391686,-1.65721984027246,339.630637695124));
#40775=CARTESIAN_POINT('Ctrl Pts',(137.896839580163,-1.52837100912795,339.676750315767));
#40776=CARTESIAN_POINT('Ctrl Pts',(137.889081768641,-1.39746176568338,339.71752904091));
#40777=CARTESIAN_POINT('Ctrl Pts',(137.881323957119,-1.26497346944824,339.752791304496));
#40778=CARTESIAN_POINT('Ctrl Pts',(137.873571983596,-1.1325848748576,339.788027032111));
#40779=CARTESIAN_POINT('Ctrl Pts',(137.865820010073,-0.998619968907839,
339.817754461025));
#40780=CARTESIAN_POINT('Ctrl Pts',(137.85806803655,-0.86357666354513,339.841840394796));
#40781=CARTESIAN_POINT('Ctrl Pts',(137.850319345992,-0.728590549102326,
339.86591612816));
#40782=CARTESIAN_POINT('Ctrl Pts',(137.842570655435,-0.592527327597096,
339.884355049795));
#40783=CARTESIAN_POINT('Ctrl Pts',(137.834821964877,-0.455896321464846,
339.897074800999));
#40784=CARTESIAN_POINT('Ctrl Pts',(137.827074886499,-0.319293742554587,
339.909791905752));
#40785=CARTESIAN_POINT('Ctrl Pts',(137.819327808121,-0.182124002937933,
339.916792170701));
#40786=CARTESIAN_POINT('Ctrl Pts',(137.811580729744,-0.0449023931984699,
339.918045021915));
#40787=CARTESIAN_POINT('Ctrl Pts',(137.803833586438,0.0923203665902042,
339.919297883629));
#40788=CARTESIAN_POINT('Ctrl Pts',(137.796086443132,0.229594606510773,339.914803231962));
#40789=CARTESIAN_POINT('Ctrl Pts',(137.788339299826,0.366404580502749,339.904582627083));
#40790=CARTESIAN_POINT('Ctrl Pts',(137.780590414798,0.503245312281391,339.894359724395));
#40791=CARTESIAN_POINT('Ctrl Pts',(137.77284152977,0.63962118072128,339.878408335994));
#40792=CARTESIAN_POINT('Ctrl Pts',(137.765092644742,0.775021502395107,339.856801903859));
#40793=CARTESIAN_POINT('Ctrl Pts',(137.757335534967,0.910565539369398,339.835172538433));
#40794=CARTESIAN_POINT('Ctrl Pts',(137.749578425192,1.04513157455788,339.807876200765));
#40795=CARTESIAN_POINT('Ctrl Pts',(137.741821315418,1.17821851810457,339.775037610961));
#40796=CARTESIAN_POINT('Ctrl Pts',(137.734060060491,1.31137657905856,339.742181473265));
#40797=CARTESIAN_POINT('Ctrl Pts',(137.726298805565,1.44305359841864,339.703777291559));
#40798=CARTESIAN_POINT('Ctrl Pts',(137.718537550639,1.57276455793385,339.659999432168));
#40799=CARTESIAN_POINT('Ctrl Pts',(137.710763880234,1.70268301271159,339.61615154247));
#40800=CARTESIAN_POINT('Ctrl Pts',(137.70299020983,1.83062875790791,339.566912937929));
#40801=CARTESIAN_POINT('Ctrl Pts',(137.695216539425,1.95613681256451,339.51250615878));
#40802=CARTESIAN_POINT('Ctrl Pts',(137.687804735248,2.0758024370805,339.460632028291));
#40803=CARTESIAN_POINT('Ctrl Pts',(137.680392931071,2.19325195341466,339.404060177001));
#40804=CARTESIAN_POINT('Ctrl Pts',(137.672981126894,2.30810550760913,339.343021071587));
#40805=CARTESIAN_POINT('Ctrl Pts',(137.665206048116,2.42858837662648,339.278990257789));
#40806=CARTESIAN_POINT('Ctrl Pts',(137.657430969337,2.54659512563419,339.209840861321));
#40807=CARTESIAN_POINT('Ctrl Pts',(137.649655890559,2.66166036226265,339.13578858));
#40808=CARTESIAN_POINT('Ctrl Pts',(137.64189037951,2.77658400379202,339.061827424726));
#40809=CARTESIAN_POINT('Ctrl Pts',(137.634124868461,2.88857300959695,338.982975598673));
#40810=CARTESIAN_POINT('Ctrl Pts',(137.626359357412,2.99718528132519,338.899495281688));
#40811=CARTESIAN_POINT('Ctrl Pts',(137.618601545889,3.10568986366975,338.816097735681));
#40812=CARTESIAN_POINT('Ctrl Pts',(137.610843734367,3.21082406681668,338.7280810681));
#40813=CARTESIAN_POINT('Ctrl Pts',(137.603085922845,3.31217387582342,338.635751267457));
#40814=CARTESIAN_POINT('Ctrl Pts',(137.595333949322,3.41344741588479,338.543490947917));
#40815=CARTESIAN_POINT('Ctrl Pts',(137.587581975799,3.51094194257992,338.446924218033));
#40816=CARTESIAN_POINT('Ctrl Pts',(137.579830002276,3.60427599945385,338.346397702345));
#40817=CARTESIAN_POINT('Ctrl Pts',(137.572081311718,3.69757052929937,338.245913759696));
#40818=CARTESIAN_POINT('Ctrl Pts',(137.564332621161,3.78670782834184,338.141473652473));
#40819=CARTESIAN_POINT('Ctrl Pts',(137.556583930603,3.87134301579653,338.033461111757));
#40820=CARTESIAN_POINT('Ctrl Pts',(137.548836852225,3.95596059419359,337.925471043953));
#40821=CARTESIAN_POINT('Ctrl Pts',(137.541089773848,4.0360776832385,337.813910328561));
#40822=CARTESIAN_POINT('Ctrl Pts',(137.53334269547,4.11138971935707,337.699195739117));
#40823=CARTESIAN_POINT('Ctrl Pts',(137.525595552164,4.18670238666302,337.584480188254));
#40824=CARTESIAN_POINT('Ctrl Pts',(137.517848408858,4.25720970620255,337.466611037367));
#40825=CARTESIAN_POINT('Ctrl Pts',(137.510101265552,4.32265070859431,337.346033655767));
#40826=CARTESIAN_POINT('Ctrl Pts',(137.502352380524,4.38810642351268,337.22542916581));
#40827=CARTESIAN_POINT('Ctrl Pts',(137.494603495496,4.44849336835652,337.102115577034));
#40828=CARTESIAN_POINT('Ctrl Pts',(137.486854610468,4.50359694194783,336.976562077694));
#40829=CARTESIAN_POINT('Ctrl Pts',(137.479097500693,4.55875900304154,336.850875314573));
#40830=CARTESIAN_POINT('Ctrl Pts',(137.471340390919,4.60862633339258,336.722944250167));
#40831=CARTESIAN_POINT('Ctrl Pts',(137.463583281144,4.6530326443263,336.593257754833));
#40832=CARTESIAN_POINT('Ctrl Pts',(137.455822026218,4.69746268457272,336.463501959182));
#40833=CARTESIAN_POINT('Ctrl Pts',(137.448060771292,4.73642577966011,336.331989238043));
#40834=CARTESIAN_POINT('Ctrl Pts',(137.440299516365,4.76980608674607,336.199221813236));
#40835=CARTESIAN_POINT('Ctrl Pts',(137.432525845961,4.80323979144476,336.066242003817));
#40836=CARTESIAN_POINT('Ctrl Pts',(137.424752175556,4.83107278267786,335.932003862852));
#40837=CARTESIAN_POINT('Ctrl Pts',(137.416978505151,4.85324057139962,335.797018832036));
#40838=CARTESIAN_POINT('Ctrl Pts',(137.409566700974,4.8743764442233,335.66831738688));
#40839=CARTESIAN_POINT('Ctrl Pts',(137.402154896797,4.89036264010635,335.538937308092));
#40840=CARTESIAN_POINT('Ctrl Pts',(137.39474309262,4.90118740262167,335.409322741712));
#40841=CARTESIAN_POINT('Ctrl Pts',(137.386968013842,4.91254271899308,335.273355379333));
#40842=CARTESIAN_POINT('Ctrl Pts',(137.379192935063,4.91825373937873,335.136700280308));
#40843=CARTESIAN_POINT('Ctrl Pts',(137.371417856285,4.91824999816171,334.999865529476));
#40844=CARTESIAN_POINT('Ctrl Pts',(137.363652345236,4.91824626154849,334.863199162517));
#40845=CARTESIAN_POINT('Ctrl Pts',(137.355886834187,4.91254175575894,334.72635397076));
#40846=CARTESIAN_POINT('Ctrl Pts',(137.348121323138,4.90111770863511,334.589843604703));
#40847=CARTESIAN_POINT('Ctrl Pts',(137.340363511615,4.88970498848726,334.45346858907));
#40848=CARTESIAN_POINT('Ctrl Pts',(137.332605700093,4.87258404488704,334.317428125481));
#40849=CARTESIAN_POINT('Ctrl Pts',(137.324847888571,4.84978814286073,334.182235955873));
#40850=CARTESIAN_POINT('Ctrl Pts',(137.317095915048,4.8270093954736,334.047145522659));
#40851=CARTESIAN_POINT('Ctrl Pts',(137.309343941525,4.79856425478291,333.912902496669));
#40852=CARTESIAN_POINT('Ctrl Pts',(137.301591968002,4.76453777678333,333.7800152312));
#40853=CARTESIAN_POINT('Ctrl Pts',(137.293843277444,4.73052570901736,333.647184243566));
#40854=CARTESIAN_POINT('Ctrl Pts',(137.286094586887,4.69093710193018,333.51570825235));
#40855=CARTESIAN_POINT('Ctrl Pts',(137.278345896329,4.64590800839346,333.386084934067));
#40856=CARTESIAN_POINT('Ctrl Pts',(137.270598817951,4.60088828353574,333.256488584998));
#40857=CARTESIAN_POINT('Ctrl Pts',(137.262851739573,4.55043045191868,333.128744511146));
#40858=CARTESIAN_POINT('Ctrl Pts',(137.255104661196,4.49472017047414,333.003334366592));
#40859=CARTESIAN_POINT('Ctrl Pts',(137.24735751789,4.43900942212383,332.87792317098));
#40860=CARTESIAN_POINT('Ctrl Pts',(137.239610374584,4.3780462948272,332.754846300897));
#40861=CARTESIAN_POINT('Ctrl Pts',(137.231863231278,4.3120640836314,332.63456422595));
#40862=CARTESIAN_POINT('Ctrl Pts',(137.22411434625,4.24606703823373,332.514255109039));
#40863=CARTESIAN_POINT('Ctrl Pts',(137.216365461222,4.17504885150819,332.396742380201));
#40864=CARTESIAN_POINT('Ctrl Pts',(137.208616576194,4.09928794085967,332.282460406834));
#40865=CARTESIAN_POINT('Ctrl Pts',(137.200859466419,4.02344661679774,332.1680571334));
#40866=CARTESIAN_POINT('Ctrl Pts',(137.193102356644,3.94285272928874,332.056891791802));
#40867=CARTESIAN_POINT('Ctrl Pts',(137.18534524687,3.85782739150161,331.949368773536));
#40868=CARTESIAN_POINT('Ctrl Pts',(137.177583991943,3.77275661889258,331.841788298406));
#40869=CARTESIAN_POINT('Ctrl Pts',(137.169822737017,3.68324993243985,331.7378543209));
#40870=CARTESIAN_POINT('Ctrl Pts',(137.162061482091,3.58966697197622,331.637936036777));
#40871=CARTESIAN_POINT('Ctrl Pts',(137.154287811686,3.49593430927446,331.537857915963));
#40872=CARTESIAN_POINT('Ctrl Pts',(137.146514141282,3.3981126213039,331.441808599185));
#40873=CARTESIAN_POINT('Ctrl Pts',(137.138740470877,3.29659709157677,331.350119087106));
#40874=CARTESIAN_POINT('Ctrl Pts',(137.1313286667,3.19980713418204,331.262697743874));
#40875=CARTESIAN_POINT('Ctrl Pts',(137.123916862523,3.09965971360733,331.179239626247));
#40876=CARTESIAN_POINT('Ctrl Pts',(137.116505058346,2.99652195965593,331.099994973362));
#40877=CARTESIAN_POINT('Ctrl Pts',(137.108729979568,2.88832911715145,331.016866303982));
#40878=CARTESIAN_POINT('Ctrl Pts',(137.100954900789,2.77650348980156,330.93811186975));
#40879=CARTESIAN_POINT('Ctrl Pts',(137.093179822011,2.66143420399861,330.864065880567));
#40880=CARTESIAN_POINT('Ctrl Pts',(137.085414310962,2.54650651827747,330.790111009689));
#40881=CARTESIAN_POINT('Ctrl Pts',(137.077648799913,2.42834344165802,330.720853264873));
#40882=CARTESIAN_POINT('Ctrl Pts',(137.069883288864,2.30736675510891,330.656586397784));
#40883=CARTESIAN_POINT('Ctrl Pts',(137.062125477341,2.1865100172968,330.59238325148));
#40884=CARTESIAN_POINT('Ctrl Pts',(137.054367665819,2.06284556418658,330.533161317365));
#40885=CARTESIAN_POINT('Ctrl Pts',(137.046609854297,1.93682341394976,330.479170637408));
#40886=CARTESIAN_POINT('Ctrl Pts',(137.038857880774,1.81089609937739,330.42522058715));
#40887=CARTESIAN_POINT('Ctrl Pts',(137.031105907251,1.68261497706301,330.37649410858));
#40888=CARTESIAN_POINT('Ctrl Pts',(137.023353933728,1.55245356082002,330.333194775438));
#40889=CARTESIAN_POINT('Ctrl Pts',(137.01560524317,1.42234726801413,330.289913779589));
#40890=CARTESIAN_POINT('Ctrl Pts',(137.007856552613,1.29036263519437,330.252055480937));
#40891=CARTESIAN_POINT('Ctrl Pts',(137.000107862055,1.15699179517662,330.219774791038));
#40892=CARTESIAN_POINT('Ctrl Pts',(136.992360783677,1.02364870407606,330.187500817407));
#40893=CARTESIAN_POINT('Ctrl Pts',(136.984613705299,0.888920359115701,330.160802236169));
#40894=CARTESIAN_POINT('Ctrl Pts',(136.976866626922,0.75331226310739,330.139783575112));
#40895=CARTESIAN_POINT('Ctrl Pts',(136.969119483616,0.617703030572713,330.118764737898));
#40896=CARTESIAN_POINT('Ctrl Pts',(136.96137234031,0.481214418545881,330.103425975681));
#40897=CARTESIAN_POINT('Ctrl Pts',(136.953625197004,0.344359895081198,330.093820292207));
#40898=CARTESIAN_POINT('Ctrl Pts',(136.945876311976,0.207474603814183,330.084212449171));
#40899=CARTESIAN_POINT('Ctrl Pts',(136.938127426948,0.070223627250653,330.080340277042));
#40900=CARTESIAN_POINT('Ctrl Pts',(136.93037854192,-0.0668770981646875,
330.082204709807));
#40901=CARTESIAN_POINT('Ctrl Pts',(136.922621432145,-0.204123343706593,
330.084071121501));
#40902=CARTESIAN_POINT('Ctrl Pts',(136.914864322371,-0.341218628072329,
330.091686295898));
#40903=CARTESIAN_POINT('Ctrl Pts',(136.907107212596,-0.47764911706483,330.104999041525));
#40904=CARTESIAN_POINT('Ctrl Pts',(136.89934595767,-0.614152510148492,330.118318901059));
#40905=CARTESIAN_POINT('Ctrl Pts',(136.891584702743,-0.74999001310014,330.137342344279));
#40906=CARTESIAN_POINT('Ctrl Pts',(136.883823447817,-0.884656539578058,
330.161966735389));
#40907=CARTESIAN_POINT('Ctrl Pts',(136.876049777413,-1.01953848861058,330.1866305175));
#40908=CARTESIAN_POINT('Ctrl Pts',(136.868276107008,-1.15324533657983,330.216913065231));
#40909=CARTESIAN_POINT('Ctrl Pts',(136.860502436603,-1.28528488149189,330.252661183789));
#40910=CARTESIAN_POINT('Ctrl Pts',(136.853090632426,-1.41117795382149,330.286745218827));
#40911=CARTESIAN_POINT('Ctrl Pts',(136.845678828249,-1.53555518116635,330.325797345066));
#40912=CARTESIAN_POINT('Ctrl Pts',(136.838267024072,-1.65800745709441,330.369644253978));
#40913=CARTESIAN_POINT('Ctrl Pts',(136.830491945294,-1.78646148383199,330.415640230509));
#40914=CARTESIAN_POINT('Ctrl Pts',(136.822716866515,-1.91320303124183,330.467058242951));
#40915=CARTESIAN_POINT('Ctrl Pts',(136.814941787737,-2.03774047646905,330.523751926774));
#40916=CARTESIAN_POINT('Ctrl Pts',(136.807176276688,-2.16212467044152,330.580375845409));
#40917=CARTESIAN_POINT('Ctrl Pts',(136.799410765639,-2.2843098065612,330.642262357709));
#40918=CARTESIAN_POINT('Ctrl Pts',(136.79164525459,-2.40382061290231,330.709215744938));
#40919=CARTESIAN_POINT('Ctrl Pts',(136.783887443068,-2.5232129239311,330.776102747689));
#40920=CARTESIAN_POINT('Ctrl Pts',(136.776129631545,-2.63993584321648,330.848046437871));
#40921=CARTESIAN_POINT('Ctrl Pts',(136.768371820023,-2.75353557447544,330.924803697661));
#40922=CARTESIAN_POINT('Ctrl Pts',(136.7606198465,-2.86704981833406,331.001503195178));
#40923=CARTESIAN_POINT('Ctrl Pts',(136.752867872977,-2.97744522975045,331.083008834211));
#40924=CARTESIAN_POINT('Ctrl Pts',(136.745115899454,-3.08429437372997,331.169032592324));
#40925=CARTESIAN_POINT('Ctrl Pts',(136.737367208897,-3.19109826703358,331.255019919323));
#40926=CARTESIAN_POINT('Ctrl Pts',(136.729618518339,-3.29435857613724,331.34552131512));
#40927=CARTESIAN_POINT('Ctrl Pts',(136.721869827781,-3.39367871130215,331.440206766264));
#40928=CARTESIAN_POINT('Ctrl Pts',(136.714122749403,-3.49297818208337,331.534872517308));
#40929=CARTESIAN_POINT('Ctrl Pts',(136.706375671026,-3.58833882680404,331.633720322616));
#40930=CARTESIAN_POINT('Ctrl Pts',(136.698628592648,-3.67939918924155,331.736381660073));
#40931=CARTESIAN_POINT('Ctrl Pts',(136.690881449342,-3.77046031485257,331.83904385793));
#40932=CARTESIAN_POINT('Ctrl Pts',(136.683134306036,-3.85722082692128,331.945519359267));
#40933=CARTESIAN_POINT('Ctrl Pts',(136.67538716273,-3.93935828644084,332.05540506121));
#40934=CARTESIAN_POINT('Ctrl Pts',(136.667638277702,-4.02151421220511,332.165315467791));
#40935=CARTESIAN_POINT('Ctrl Pts',(136.659889392674,-4.09904478323544,332.27863728758));
#40936=CARTESIAN_POINT('Ctrl Pts',(136.652140507646,-4.17167001130741,332.394937164048));
#40937=CARTESIAN_POINT('Ctrl Pts',(136.644383397872,-4.2443723245468,332.511360482406));
#40938=CARTESIAN_POINT('Ctrl Pts',(136.636626288097,-4.31215868682998,332.630767839654));
#40939=CARTESIAN_POINT('Ctrl Pts',(136.628869178322,-4.37479408099023,332.752699439008));
#40940=CARTESIAN_POINT('Ctrl Pts',(136.621107923396,-4.43746294550244,332.874696194711));
#40941=CARTESIAN_POINT('Ctrl Pts',(136.61334666847,-4.49497519345254,332.999219525601));
#40942=CARTESIAN_POINT('Ctrl Pts',(136.605585413544,-4.54714380227066,333.125789151677));
#40943=CARTESIAN_POINT('Ctrl Pts',(136.597811743139,-4.59939586386118,333.252561247906));
#40944=CARTESIAN_POINT('Ctrl Pts',(136.590038072734,-4.64628707095768,333.381385813063));
#40945=CARTESIAN_POINT('Ctrl Pts',(136.58226440233,-4.68767988958946,333.511766041498));
#40946=CARTESIAN_POINT('Ctrl Pts',(136.574852598153,-4.72714586255579,333.636077038933));
#40947=CARTESIAN_POINT('Ctrl Pts',(136.567440793975,-4.76161375094119,333.761801849198));
#40948=CARTESIAN_POINT('Ctrl Pts',(136.560028989798,-4.79100790261916,333.888502658779));
#40949=CARTESIAN_POINT('Ctrl Pts',(136.549446866247,-4.83297508595386,334.069398374451));
#40950=CARTESIAN_POINT('Ctrl Pts',(136.538864742696,-4.86471113811121,334.252750046396));
#40951=CARTESIAN_POINT('Ctrl Pts',(136.528282619144,-4.88598650972011,334.437577659287));
#40952=CARTESIAN_POINT('Ctrl Pts',(136.517700495593,-4.907261881329,334.622405272178));
#40953=CARTESIAN_POINT('Ctrl Pts',(136.507118372042,-4.91807642230174,334.808709451141));
#40954=CARTESIAN_POINT('Ctrl Pts',(136.49653624849,-4.91824792654155,334.995483854551));
#40955=CARTESIAN_POINT('',(139.996536248436,-4.91824872290583,335.003544310248));
#40956=CARTESIAN_POINT('Ctrl Pts',(139.996536248436,-4.91824872290583,335.003544310248));
#40957=CARTESIAN_POINT('Ctrl Pts',(139.987647616362,-4.91813521599565,335.161051745276));
#40958=CARTESIAN_POINT('Ctrl Pts',(139.978758984289,-4.91045146808829,335.318255606896));
#40959=CARTESIAN_POINT('Ctrl Pts',(139.969870352215,-4.89530859694114,335.474485830362));
#40960=CARTESIAN_POINT('Ctrl Pts',(139.960938083389,-4.88009138525247,335.631483031193));
#40961=CARTESIAN_POINT('Ctrl Pts',(139.952005814563,-4.85734174321484,335.787496869337));
#40962=CARTESIAN_POINT('Ctrl Pts',(139.943073545737,-4.82722190234324,335.941866109401));
#40963=CARTESIAN_POINT('Ctrl Pts',(139.934085617475,-4.79691437641931,336.097197266861));
#40964=CARTESIAN_POINT('Ctrl Pts',(139.925097689213,-4.75914460223028,336.250863127016));
#40965=CARTESIAN_POINT('Ctrl Pts',(139.916109760952,-4.71412634167529,336.402211074419));
#40966=CARTESIAN_POINT('Ctrl Pts',(139.910368307663,-4.68536885356579,336.498891549057));
#40967=CARTESIAN_POINT('Ctrl Pts',(139.904626854374,-4.65365451630116,336.594626606268));
#40968=CARTESIAN_POINT('Ctrl Pts',(139.898885401086,-4.61904906007375,336.689250971032));
#40969=CARTESIAN_POINT('Ctrl Pts',(139.891110322307,-4.57218633476673,336.817391330868));
#40970=CARTESIAN_POINT('Ctrl Pts',(139.883335243529,-4.51991326629705,336.943782620743));
#40971=CARTESIAN_POINT('Ctrl Pts',(139.87556016475,-4.46237953711759,337.067934217816));
#40972=CARTESIAN_POINT('Ctrl Pts',(139.867794653701,-4.40491660685465,337.191933038445));
#40973=CARTESIAN_POINT('Ctrl Pts',(139.860029142652,-4.34220605922225,337.313697298837));
#40974=CARTESIAN_POINT('Ctrl Pts',(139.852263631603,-4.27444681928786,337.432753060132));
#40975=CARTESIAN_POINT('Ctrl Pts',(139.844505820081,-4.2067547628372,337.551690777292));
#40976=CARTESIAN_POINT('Ctrl Pts',(139.836748008559,-4.13402416799171,337.667925002101));
#40977=CARTESIAN_POINT('Ctrl Pts',(139.828990197037,-4.05650121274327,337.781003591064));
#40978=CARTESIAN_POINT('Ctrl Pts',(139.821238223514,-3.97903659597706,337.893997084804));
#40979=CARTESIAN_POINT('Ctrl Pts',(139.813486249991,-3.89678701730541,338.003839348365));
#40980=CARTESIAN_POINT('Ctrl Pts',(139.805734276467,-3.81004338021991,338.110104902305));
#40981=CARTESIAN_POINT('Ctrl Pts',(139.79798558591,-3.72333647911625,338.21632545272));
#40982=CARTESIAN_POINT('Ctrl Pts',(139.790236895352,-3.63213955166073,338.31897200405));
#40983=CARTESIAN_POINT('Ctrl Pts',(139.782488204795,-3.53678528301995,338.417650205084));
#40984=CARTESIAN_POINT('Ctrl Pts',(139.774741126417,-3.44145085363118,338.516307875295));
#40985=CARTESIAN_POINT('Ctrl Pts',(139.766994048039,-3.34196107498748,338.610998556575));
#40986=CARTESIAN_POINT('Ctrl Pts',(139.759246969661,-3.23868690268931,338.701363290579));
#40987=CARTESIAN_POINT('Ctrl Pts',(139.751499826355,-3.13541186485413,338.791728781928));
#40988=CARTESIAN_POINT('Ctrl Pts',(139.743752683049,-3.02835266426594,338.877767996294));
#40989=CARTESIAN_POINT('Ctrl Pts',(139.736005539744,-2.91791457290447,338.959161225276));
#40990=CARTESIAN_POINT('Ctrl Pts',(139.728256654715,-2.80745165271555,339.040572753185));
#40991=CARTESIAN_POINT('Ctrl Pts',(139.720507769687,-2.69360864473185,339.117335985385));
#40992=CARTESIAN_POINT('Ctrl Pts',(139.712758884659,-2.57682078711325,339.189173867674));
#40993=CARTESIAN_POINT('Ctrl Pts',(139.705001774885,-2.45990896965572,339.261087999433));
#40994=CARTESIAN_POINT('Ctrl Pts',(139.69724466511,-2.34004639215398,339.328066133112));
#40995=CARTESIAN_POINT('Ctrl Pts',(139.689487555335,-2.21769442860519,339.38987636316));
#40996=CARTESIAN_POINT('Ctrl Pts',(139.681726300409,-2.09527708407922,339.451719622619));
#40997=CARTESIAN_POINT('Ctrl Pts',(139.673965045483,-1.97036805863983,339.508389314376));
#40998=CARTESIAN_POINT('Ctrl Pts',(139.666203790557,-1.843448884797,339.559701664763));
#40999=CARTESIAN_POINT('Ctrl Pts',(139.658430120152,-1.71632668163883,339.611096098187));
#41000=CARTESIAN_POINT('Ctrl Pts',(139.650656449747,-1.58718827277892,339.657115933564));
#41001=CARTESIAN_POINT('Ctrl Pts',(139.642882779343,-1.4565313816709,339.697626996336));
#41002=CARTESIAN_POINT('Ctrl Pts',(139.635470975165,-1.33195660027659,339.736252259391));
#41003=CARTESIAN_POINT('Ctrl Pts',(139.628059170988,-1.20600180393444,339.769870000609));
#41004=CARTESIAN_POINT('Ctrl Pts',(139.620647366811,-1.07910530725297,339.798407527332));
#41005=CARTESIAN_POINT('Ctrl Pts',(139.612872288033,-0.945989235265604,
339.828343763249));
#41006=CARTESIAN_POINT('Ctrl Pts',(139.605097209254,-0.811416146393164,
339.852783804057));
#41007=CARTESIAN_POINT('Ctrl Pts',(139.597322130476,-0.675879617612291,
339.871588016756));
#41008=CARTESIAN_POINT('Ctrl Pts',(139.589556619427,-0.540509875158715,
339.890369089673));
#41009=CARTESIAN_POINT('Ctrl Pts',(139.581791108378,-0.404179435214022,
339.903528080428));
#41010=CARTESIAN_POINT('Ctrl Pts',(139.574025597329,-0.26739449284549,339.910975793841));
#41011=CARTESIAN_POINT('Ctrl Pts',(139.566267785806,-0.130745173145602,
339.918416122825));
#41012=CARTESIAN_POINT('Ctrl Pts',(139.558509974284,0.00635736439610471,
339.920156422543));
#41013=CARTESIAN_POINT('Ctrl Pts',(139.550752162762,0.143399681632911,339.916159028531));
#41014=CARTESIAN_POINT('Ctrl Pts',(139.543000189239,0.280338870180042,339.912164642685));
#41015=CARTESIAN_POINT('Ctrl Pts',(139.535248215716,0.417217539489989,339.902441168823));
#41016=CARTESIAN_POINT('Ctrl Pts',(139.527496242193,0.553520470249815,339.887002982556));
#41017=CARTESIAN_POINT('Ctrl Pts',(139.519747551635,0.689765676637587,339.871571334371));
#41018=CARTESIAN_POINT('Ctrl Pts',(139.511998861078,0.825435241844567,339.850429831255));
#41019=CARTESIAN_POINT('Ctrl Pts',(139.50425017052,0.960017512489698,339.823644829194));
#41020=CARTESIAN_POINT('Ctrl Pts',(139.496503092142,1.09457178216941,339.796865399977));
#41021=CARTESIAN_POINT('Ctrl Pts',(139.488756013764,1.22803882414136,339.764444883585));
#41022=CARTESIAN_POINT('Ctrl Pts',(139.481008935387,1.35991603731443,339.726500971539));
#41023=CARTESIAN_POINT('Ctrl Pts',(139.473261792081,1.49179435574552,339.688556741486));
#41024=CARTESIAN_POINT('Ctrl Pts',(139.465514648775,1.62208244316626,339.645089131526));
#41025=CARTESIAN_POINT('Ctrl Pts',(139.457767505469,1.75029213403813,339.596265930951));
#41026=CARTESIAN_POINT('Ctrl Pts',(139.450018620441,1.87853064917044,339.547431753885));
#41027=CARTESIAN_POINT('Ctrl Pts',(139.442269735413,2.00468947272995,339.493239729354));
#41028=CARTESIAN_POINT('Ctrl Pts',(139.434520850385,2.12830009158425,339.433905928486));
#41029=CARTESIAN_POINT('Ctrl Pts',(139.42676374061,2.25204191202657,339.374509150109));
#41030=CARTESIAN_POINT('Ctrl Pts',(139.419006630835,2.37322977195209,339.309959862869));
#41031=CARTESIAN_POINT('Ctrl Pts',(139.411249521061,2.49141898109368,339.240520548606));
#41032=CARTESIAN_POINT('Ctrl Pts',(139.403488266134,2.60967134676968,339.171044128193));
#41033=CARTESIAN_POINT('Ctrl Pts',(139.395727011208,2.72492154050674,339.096672685799));
#41034=CARTESIAN_POINT('Ctrl Pts',(139.387965756282,2.83675443823476,339.017711701909));
#41035=CARTESIAN_POINT('Ctrl Pts',(139.380192085877,2.94876623215281,338.938624406178));
#41036=CARTESIAN_POINT('Ctrl Pts',(139.372418415473,3.05734949650549,338.85493313666));
#41037=CARTESIAN_POINT('Ctrl Pts',(139.364644745068,3.16212205432583,338.766983830075));
#41038=CARTESIAN_POINT('Ctrl Pts',(139.357232940891,3.26201742437199,338.683128584872));
#41039=CARTESIAN_POINT('Ctrl Pts',(139.349821136714,3.35844866774865,338.59540299826));
#41040=CARTESIAN_POINT('Ctrl Pts',(139.342409332537,3.45111745846367,338.504136320178));
#41041=CARTESIAN_POINT('Ctrl Pts',(139.334634253759,3.54832822265841,338.408396390332));
#41042=CARTESIAN_POINT('Ctrl Pts',(139.32685917498,3.64170559457075,338.308456917359));
#41043=CARTESIAN_POINT('Ctrl Pts',(139.319084096202,3.73086505100657,338.204657397239));
#41044=CARTESIAN_POINT('Ctrl Pts',(139.311318585153,3.81991479105509,338.100985609036));
#41045=CARTESIAN_POINT('Ctrl Pts',(139.303553074104,3.90475669080866,337.993463518565));
#41046=CARTESIAN_POINT('Ctrl Pts',(139.295787563055,3.98504181294203,337.882468527426));
#41047=CARTESIAN_POINT('Ctrl Pts',(139.288029751532,4.06524733214306,337.771583588145));
#41048=CARTESIAN_POINT('Ctrl Pts',(139.28027194001,4.14090483730894,337.657232915407));
#41049=CARTESIAN_POINT('Ctrl Pts',(139.272514128488,4.21170480474704,337.539827887903));
#41050=CARTESIAN_POINT('Ctrl Pts',(139.264762154965,4.28245149296448,337.422511211405));
#41051=CARTESIAN_POINT('Ctrl Pts',(139.257010181442,4.34834771841282,337.302145088565));
#41052=CARTESIAN_POINT('Ctrl Pts',(139.249258207919,4.40912675511663,337.179170557762));
#41053=CARTESIAN_POINT('Ctrl Pts',(139.241509517361,4.46988005186227,337.056248106745));
#41054=CARTESIAN_POINT('Ctrl Pts',(139.233760826804,4.52552029730964,336.930719794544));
#41055=CARTESIAN_POINT('Ctrl Pts',(139.226012136246,4.57582640661904,336.803051790434));
#41056=CARTESIAN_POINT('Ctrl Pts',(139.218265057868,4.62612204932223,336.675410348718));
#41057=CARTESIAN_POINT('Ctrl Pts',(139.210517979491,4.67108562017492,336.545630464021));
#41058=CARTESIAN_POINT('Ctrl Pts',(139.202770901113,4.7105441021983,336.414198473958));
#41059=CARTESIAN_POINT('Ctrl Pts',(139.195023757807,4.75000291492175,336.282765382368));
#41060=CARTESIAN_POINT('Ctrl Pts',(139.187276614501,4.78395643439791,336.149680532161));
#41061=CARTESIAN_POINT('Ctrl Pts',(139.179529471195,4.81228158383889,336.015445232568));
#41062=CARTESIAN_POINT('Ctrl Pts',(139.171780586167,4.84061310137481,335.88117975403));
#41063=CARTESIAN_POINT('Ctrl Pts',(139.164031701139,4.86331365023053,335.745763693807));
#41064=CARTESIAN_POINT('Ctrl Pts',(139.156282816111,4.88031138988746,335.609707963073));
#41065=CARTESIAN_POINT('Ctrl Pts',(139.148525706336,4.8973271711209,335.473507821381));
#41066=CARTESIAN_POINT('Ctrl Pts',(139.140768596562,4.90862800314639,335.336667041378));
#41067=CARTESIAN_POINT('Ctrl Pts',(139.133011486787,4.9141939651214,335.199701616579));
#41068=CARTESIAN_POINT('Ctrl Pts',(139.125250231861,4.91976290136852,335.062663001838));
#41069=CARTESIAN_POINT('Ctrl Pts',(139.117488976935,4.91959086170075,334.925500000258));
#41070=CARTESIAN_POINT('Ctrl Pts',(139.109727722008,4.91371008371975,334.788727011545));
#41071=CARTESIAN_POINT('Ctrl Pts',(139.101954051604,4.90781989841053,334.651735230624));
#41072=CARTESIAN_POINT('Ctrl Pts',(139.094180381199,4.89620275924597,334.515135098968));
#41073=CARTESIAN_POINT('Ctrl Pts',(139.086406710795,4.87894275390741,334.379435203549));
#41074=CARTESIAN_POINT('Ctrl Pts',(139.078994906617,4.8624862059697,334.250052170908));
#41075=CARTESIAN_POINT('Ctrl Pts',(139.07158310244,4.84090036765922,334.121487732471));
#41076=CARTESIAN_POINT('Ctrl Pts',(139.064171298263,4.81430067095986,333.994170932964));
#41077=CARTESIAN_POINT('Ctrl Pts',(139.056396219485,4.78639724388913,333.860613957856));
#41078=CARTESIAN_POINT('Ctrl Pts',(139.048621140706,4.75288786288529,333.728007950344));
#41079=CARTESIAN_POINT('Ctrl Pts',(139.040846061928,4.71384992979645,333.596859984942));
#41080=CARTESIAN_POINT('Ctrl Pts',(139.033080550879,4.67486003536955,333.465873405459));
#41081=CARTESIAN_POINT('Ctrl Pts',(139.02531503983,4.63035523579267,333.336341669164));
#41082=CARTESIAN_POINT('Ctrl Pts',(139.017549528781,4.58046406611567,333.208762438557));
#41083=CARTESIAN_POINT('Ctrl Pts',(139.009791717258,4.53062236367866,333.08130970313));
#41084=CARTESIAN_POINT('Ctrl Pts',(139.002033905736,4.47540506068098,332.955805982495));
#41085=CARTESIAN_POINT('Ctrl Pts',(138.994276094214,4.41499059320829,332.832734182344));
#41086=CARTESIAN_POINT('Ctrl Pts',(138.986524120691,4.35462158953825,332.709754997625));
#41087=CARTESIAN_POINT('Ctrl Pts',(138.978772147168,4.28906337765768,332.589204440135));
#41088=CARTESIAN_POINT('Ctrl Pts',(138.971020173645,4.21854249541944,332.471545476612));
#41089=CARTESIAN_POINT('Ctrl Pts',(138.963271483087,4.14805147881671,332.35393634173));
#41090=CARTESIAN_POINT('Ctrl Pts',(138.95552279253,4.07260217250614,332.239216699756));
#41091=CARTESIAN_POINT('Ctrl Pts',(138.947774101972,3.99246694648356,332.127824736591));
#41092=CARTESIAN_POINT('Ctrl Pts',(138.940027023594,3.91234839326405,332.016455949455));
#41093=CARTESIAN_POINT('Ctrl Pts',(138.932279945216,3.82754608768726,331.908413781091));
#41094=CARTESIAN_POINT('Ctrl Pts',(138.924532866839,3.73837537201439,331.804106910359));
#41095=CARTESIAN_POINT('Ctrl Pts',(138.916785723533,3.64920390900509,331.699799165434));
#41096=CARTESIAN_POINT('Ctrl Pts',(138.909038580227,3.55566421686661,331.599227077686));
#41097=CARTESIAN_POINT('Ctrl Pts',(138.901291436921,3.4581112533133,331.502765432201));
#41098=CARTESIAN_POINT('Ctrl Pts',(138.893542551893,3.36053635778264,331.40628210009));
#41099=CARTESIAN_POINT('Ctrl Pts',(138.885793666865,3.25894667330923,331.313911323904));
#41100=CARTESIAN_POINT('Ctrl Pts',(138.878044781837,3.15373295897183,331.225989999219));
#41101=CARTESIAN_POINT('Ctrl Pts',(138.870287672062,3.04840756971094,331.137975353932));
#41102=CARTESIAN_POINT('Ctrl Pts',(138.862530562288,2.93945076708657,331.054419845207));
#41103=CARTESIAN_POINT('Ctrl Pts',(138.854773452513,2.82728568074394,330.975619458605));
#41104=CARTESIAN_POINT('Ctrl Pts',(138.847012197587,2.71506065696551,330.896776963596));
#41105=CARTESIAN_POINT('Ctrl Pts',(138.83925094266,2.59962426215665,330.822694864856));
#41106=CARTESIAN_POINT('Ctrl Pts',(138.831489687734,2.48142651161956,330.753624424296));
#41107=CARTESIAN_POINT('Ctrl Pts',(138.82371601733,2.36303968320221,330.684443493542));
#41108=CARTESIAN_POINT('Ctrl Pts',(138.815942346925,2.24188301766289,330.620290424353));
#41109=CARTESIAN_POINT('Ctrl Pts',(138.80816867652,2.11842970130722,330.561369731199));
#41110=CARTESIAN_POINT('Ctrl Pts',(138.800756872343,2.0007231665291,330.505191810486));
#41111=CARTESIAN_POINT('Ctrl Pts',(138.793345068166,1.88092925174198,330.453770207772));
#41112=CARTESIAN_POINT('Ctrl Pts',(138.785933263989,1.75947121667798,330.407240034556));
#41113=CARTESIAN_POINT('Ctrl Pts',(138.778158185211,1.63206016151062,330.358429278945));
#41114=CARTESIAN_POINT('Ctrl Pts',(138.770383106432,1.50241509194013,330.314847312727));
#41115=CARTESIAN_POINT('Ctrl Pts',(138.762608027654,1.37100430432327,330.276703454151));
#41116=CARTESIAN_POINT('Ctrl Pts',(138.754842516605,1.23975522604655,330.238606534022));
#41117=CARTESIAN_POINT('Ctrl Pts',(138.747077005556,1.10674512482111,330.205934514415));
#41118=CARTESIAN_POINT('Ctrl Pts',(138.739311494507,0.972462053353817,330.178848621202));
#41119=CARTESIAN_POINT('Ctrl Pts',(138.731553682985,0.838312123942887,330.151789583731));
#41120=CARTESIAN_POINT('Ctrl Pts',(138.723795871462,0.702892116736589,330.130305727194));
#41121=CARTESIAN_POINT('Ctrl Pts',(138.71603805994,0.566704679436738,330.114508328857));
#41122=CARTESIAN_POINT('Ctrl Pts',(138.708286086417,0.430619727502208,330.098722818564));
#41123=CARTESIAN_POINT('Ctrl Pts',(138.700534112894,0.293768881697937,330.08861529371));
#41124=CARTESIAN_POINT('Ctrl Pts',(138.692782139371,0.156664053261195,330.084245791649));
#41125=CARTESIAN_POINT('Ctrl Pts',(138.685033448814,0.0196172888007414,
330.079878140075));
#41126=CARTESIAN_POINT('Ctrl Pts',(138.677284758256,-0.117682854496473,
330.081243690508));
#41127=CARTESIAN_POINT('Ctrl Pts',(138.669536067698,-0.254720501724082,
330.088350528743));
#41128=CARTESIAN_POINT('Ctrl Pts',(138.66178898932,-0.391729637124671,330.09545588834));
#41129=CARTESIAN_POINT('Ctrl Pts',(138.654041910943,-0.528475994983113,
330.108300139518));
#41130=CARTESIAN_POINT('Ctrl Pts',(138.646294832565,-0.664445258736857,
330.12683926382));
#41131=CARTESIAN_POINT('Ctrl Pts',(138.638547689259,-0.800415662043992,
330.145378543499));
#41132=CARTESIAN_POINT('Ctrl Pts',(138.630800545953,-0.935608570965312,
330.169612738694));
#41133=CARTESIAN_POINT('Ctrl Pts',(138.623053402647,-1.0695167327395,330.199446175607));
#41134=CARTESIAN_POINT('Ctrl Pts',(138.615304517619,-1.2034549999114,330.229286319711));
#41135=CARTESIAN_POINT('Ctrl Pts',(138.607555632591,-1.33610756373403,330.264728125477));
#41136=CARTESIAN_POINT('Ctrl Pts',(138.599806747563,-1.46697965937024,330.305625308788));
#41137=CARTESIAN_POINT('Ctrl Pts',(138.592049637788,-1.59799066400087,330.346565900792));
#41138=CARTESIAN_POINT('Ctrl Pts',(138.584292528014,-1.72721705170641,330.392973320425));
#41139=CARTESIAN_POINT('Ctrl Pts',(138.576535418239,-1.85418094218393,330.444651923712));
#41140=CARTESIAN_POINT('Ctrl Pts',(138.568774163313,-1.98121267810497,330.496358142392));
#41141=CARTESIAN_POINT('Ctrl Pts',(138.561012908387,-2.10597915237709,330.553340995057));
#41142=CARTESIAN_POINT('Ctrl Pts',(138.553251653461,-2.22802554439818,330.615358026474));
#41143=CARTESIAN_POINT('Ctrl Pts',(138.545477983056,-2.35026717087167,330.67747426493));
#41144=CARTESIAN_POINT('Ctrl Pts',(138.537704312651,-2.46977967908966,330.744640582905));
#41145=CARTESIAN_POINT('Ctrl Pts',(138.529930642247,-2.5861350202107,330.816569742455));
#41146=CARTESIAN_POINT('Ctrl Pts',(138.52251883807,-2.69707399220891,330.885150582323));
#41147=CARTESIAN_POINT('Ctrl Pts',(138.515107033892,-2.80514287602787,330.958060661159));
#41148=CARTESIAN_POINT('Ctrl Pts',(138.507695229715,-2.90999900339613,331.03501716741));
#41149=CARTESIAN_POINT('Ctrl Pts',(138.499989985559,-3.01900647894815,331.115020450807));
#41150=CARTESIAN_POINT('Ctrl Pts',(138.492284741403,-3.12489967861004,331.199660154725));
#41151=CARTESIAN_POINT('Ctrl Pts',(138.484579497247,-3.22725339229766,331.288663501594));
#41152=CARTESIAN_POINT('Ctrl Pts',(138.47688376838,-3.32948070828308,331.377556937271));
#41153=CARTESIAN_POINT('Ctrl Pts',(138.469188039513,-3.42817693442612,331.470803038781));
#41154=CARTESIAN_POINT('Ctrl Pts',(138.461492310646,-3.52294624608198,331.568086130201));
#41155=CARTESIAN_POINT('Ctrl Pts',(138.453804161778,-3.6176222135787,331.665273401485));
#41156=CARTESIAN_POINT('Ctrl Pts',(138.446116012911,-3.70837868497844,331.766489468646));
#41157=CARTESIAN_POINT('Ctrl Pts',(138.438427864043,-3.79485368309668,331.871379123897));
#41158=CARTESIAN_POINT('Ctrl Pts',(138.430432380063,-3.88478553457888,331.980461761692));
#41159=CARTESIAN_POINT('Ctrl Pts',(138.422436896083,-3.97008616230015,332.093517512434));
#41160=CARTESIAN_POINT('Ctrl Pts',(138.414441412103,-4.05039117206293,332.210104945383));
#41161=CARTESIAN_POINT('Ctrl Pts',(138.406762059569,-4.12752102208044,332.322082656909));
#41162=CARTESIAN_POINT('Ctrl Pts',(138.399082707035,-4.20004250895292,332.437317741729));
#41163=CARTESIAN_POINT('Ctrl Pts',(138.391403354502,-4.26767479704982,332.555386556299));
#41164=CARTESIAN_POINT('Ctrl Pts',(138.383725265561,-4.33529595664338,332.673435943325));
#41165=CARTESIAN_POINT('Ctrl Pts',(138.37604717662,-4.39802931932651,332.794317787035));
#41166=CARTESIAN_POINT('Ctrl Pts',(138.36836908768,-4.45563881475275,332.917581738706));
#41167=CARTESIAN_POINT('Ctrl Pts',(138.360690526208,-4.51325185562625,333.040853276381));
#41168=CARTESIAN_POINT('Ctrl Pts',(138.353011964737,-4.56574023362412,333.166506852295));
#41169=CARTESIAN_POINT('Ctrl Pts',(138.345333403266,-4.61291526543899,333.294070395245));
#41170=CARTESIAN_POINT('Ctrl Pts',(138.337652633093,-4.66010386692659,333.421670631239));
#41171=CARTESIAN_POINT('Ctrl Pts',(138.32997186292,-4.70197594459933,333.551181553172));
#41172=CARTESIAN_POINT('Ctrl Pts',(138.322291092747,-4.73839225483785,333.682114609766));
#41173=CARTESIAN_POINT('Ctrl Pts',(138.314602413885,-4.77484606200135,333.813182484714));
#41174=CARTESIAN_POINT('Ctrl Pts',(138.306913735024,-4.80583278181753,333.945675033012));
#41175=CARTESIAN_POINT('Ctrl Pts',(138.299225056162,-4.83126394489471,334.079091884464));
#41176=CARTESIAN_POINT('Ctrl Pts',(138.29153168722,-4.8567106209356,334.212590119955));
#41177=CARTESIAN_POINT('Ctrl Pts',(138.283838318278,-4.87659493447119,334.347013388021));
#41178=CARTESIAN_POINT('Ctrl Pts',(138.276144949336,-4.89088027700115,334.481856025278));
#41179=CARTESIAN_POINT('Ctrl Pts',(138.268441174777,-4.90518494107916,334.616881043074));
#41180=CARTESIAN_POINT('Ctrl Pts',(138.260737400219,-4.91387549554807,334.752326166009));
#41181=CARTESIAN_POINT('Ctrl Pts',(138.25303362566,-4.91696740557989,334.887685286071));
#41182=CARTESIAN_POINT('Ctrl Pts',(138.250867833281,-4.91783664638312,334.925739326789));
#41183=CARTESIAN_POINT('Ctrl Pts',(138.248702040901,-4.91826370620767,334.963786600083));
#41184=CARTESIAN_POINT('Ctrl Pts',(138.246536248522,-4.91824966475132,335.001815949749));
#41185=CARTESIAN_POINT('',(141.746536248545,-4.91824882895472,334.996606036901));
#41186=CARTESIAN_POINT('Ctrl Pts',(141.74653624849,-4.91824882895539,334.996606037877));
#41187=CARTESIAN_POINT('Ctrl Pts',(141.738756538685,-4.91834398132713,335.134492974708));
#41188=CARTESIAN_POINT('Ctrl Pts',(141.730976828881,-4.91263616094097,335.272420682955));
#41189=CARTESIAN_POINT('Ctrl Pts',(141.723197119076,-4.90114179516215,335.409868474288));
#41190=CARTESIAN_POINT('Ctrl Pts',(141.715417497372,-4.88964755954944,335.547314709114));
#41191=CARTESIAN_POINT('Ctrl Pts',(141.707637875667,-4.87236694027544,335.684280653093));
#41192=CARTESIAN_POINT('Ctrl Pts',(141.699858253963,-4.84936833957404,335.820249821479));
#41193=CARTESIAN_POINT('Ctrl Pts',(141.692077090379,-4.82636518067306,335.956245938228));
#41194=CARTESIAN_POINT('Ctrl Pts',(141.684295926795,-4.7976418484734,336.091244505456));
#41195=CARTESIAN_POINT('Ctrl Pts',(141.676514763211,-4.76331799226883,336.224738652541));
#41196=CARTESIAN_POINT('Ctrl Pts',(141.668730427127,-4.72898014169905,336.358287227248));
#41197=CARTESIAN_POINT('Ctrl Pts',(141.660946091043,-4.68903731748926,336.490329787161));
#41198=CARTESIAN_POINT('Ctrl Pts',(141.653161754958,-4.64365911135693,336.620374376498));
#41199=CARTESIAN_POINT('Ctrl Pts',(141.645367727005,-4.59822440719476,336.750580877548));
#41200=CARTESIAN_POINT('Ctrl Pts',(141.637573699051,-4.54734093321821,336.878784075261));
#41201=CARTESIAN_POINT('Ctrl Pts',(141.629779671097,-4.49122678197054,337.004511176175));
#41202=CARTESIAN_POINT('Ctrl Pts',(141.621980325694,-4.43507434702874,337.130324053988));
#41203=CARTESIAN_POINT('Ctrl Pts',(141.61418098029,-4.37368429609552,337.253657124271));
#41204=CARTESIAN_POINT('Ctrl Pts',(141.606381634887,-4.30732038762834,337.374062792097));
#41205=CARTESIAN_POINT('Ctrl Pts',(141.598569673064,-4.24084912721982,337.494663231185));
#41206=CARTESIAN_POINT('Ctrl Pts',(141.590757711242,-4.16938813773808,337.612326479504));
#41207=CARTESIAN_POINT('Ctrl Pts',(141.582945749419,-4.0932445566266,337.726633833529));
#41208=CARTESIAN_POINT('Ctrl Pts',(141.578068368523,-4.04570448201125,337.798001374432));
#41209=CARTESIAN_POINT('Ctrl Pts',(141.573190987626,-3.99633990974758,337.868061389034));
#41210=CARTESIAN_POINT('Ctrl Pts',(141.568313606729,-3.94523323621345,337.936718879017));
#41211=CARTESIAN_POINT('Ctrl Pts',(141.560538527951,-3.86376360707521,338.046166429791));
#41212=CARTESIAN_POINT('Ctrl Pts',(141.552763449172,-3.77760739456703,338.15239419871));
#41213=CARTESIAN_POINT('Ctrl Pts',(141.544988370394,-3.68704801975687,338.25497464852));
#41214=CARTESIAN_POINT('Ctrl Pts',(141.537222859345,-3.59660008402268,338.357428866555));
#41215=CARTESIAN_POINT('Ctrl Pts',(141.529457348296,-3.501760023206,338.456244405604));
#41216=CARTESIAN_POINT('Ctrl Pts',(141.521691837247,-3.40285369549707,338.551023766401));
#41217=CARTESIAN_POINT('Ctrl Pts',(141.513934025724,-3.30404543369986,338.645709153185));
#41218=CARTESIAN_POINT('Ctrl Pts',(141.506176214202,-3.20117920874914,338.736366056992));
#41219=CARTESIAN_POINT('Ctrl Pts',(141.49841840268,-3.09461995083519,338.822631347958));
#41220=CARTESIAN_POINT('Ctrl Pts',(141.490666429157,-2.98814088214216,338.908831721557));
#41221=CARTESIAN_POINT('Ctrl Pts',(141.482914455634,-2.87797461477476,338.99064681546));
#41222=CARTESIAN_POINT('Ctrl Pts',(141.475162482111,-2.76452133964631,339.067751814595));
#41223=CARTESIAN_POINT('Ctrl Pts',(141.467413791553,-2.65111611204728,339.144824159717));
#41224=CARTESIAN_POINT('Ctrl Pts',(141.459665100996,-2.5344269679848,339.217190158193));
#41225=CARTESIAN_POINT('Ctrl Pts',(141.451916410438,-2.41488526411081,339.284566748655));
#41226=CARTESIAN_POINT('Ctrl Pts',(141.44416933206,-2.29536843188661,339.351929320855));
#41227=CARTESIAN_POINT('Ctrl Pts',(141.436422253683,-2.17300056066116,339.414304358071));
#41228=CARTESIAN_POINT('Ctrl Pts',(141.428675175305,-2.04823959092459,339.471453638434));
#41229=CARTESIAN_POINT('Ctrl Pts',(141.420928031999,-1.92347757557131,339.528603397764));
#41230=CARTESIAN_POINT('Ctrl Pts',(141.413180888693,-1.79632277706827,339.580527150103));
#41231=CARTESIAN_POINT('Ctrl Pts',(141.405433745387,-1.66725482969334,339.627034081932));
#41232=CARTESIAN_POINT('Ctrl Pts',(141.397684860359,-1.53815786510339,339.673551469507));
#41233=CARTESIAN_POINT('Ctrl Pts',(141.389935975331,-1.40714726341605,339.714649480776));
#41234=CARTESIAN_POINT('Ctrl Pts',(141.382187090303,-1.27471921213646,339.750186732404));
#41235=CARTESIAN_POINT('Ctrl Pts',(141.374429980528,-1.14215060035509,339.785761703639));
#41236=CARTESIAN_POINT('Ctrl Pts',(141.366672870753,-1.00816191172415,339.815764023472));
#41237=CARTESIAN_POINT('Ctrl Pts',(141.358915760979,-0.873261504206372,
339.840103036896));
#41238=CARTESIAN_POINT('Ctrl Pts',(141.351154506053,-0.738289010224137,
339.86445505631));
#41239=CARTESIAN_POINT('Ctrl Pts',(141.343393251126,-0.602404213613322,
339.883137685947));
#41240=CARTESIAN_POINT('Ctrl Pts',(141.3356319962,-0.466121062823814,339.896112153259));
#41241=CARTESIAN_POINT('Ctrl Pts',(141.327858325796,-0.329619903407525,
339.909107375491));
#41242=CARTESIAN_POINT('Ctrl Pts',(141.320084655391,-0.192719506954368,
339.916376167823));
#41243=CARTESIAN_POINT('Ctrl Pts',(141.312310984986,-0.0559351911396397,
339.917931914626));
#41244=CARTESIAN_POINT('Ctrl Pts',(141.304899180809,0.0744817818656994,
339.91941524104));
#41245=CARTESIAN_POINT('Ctrl Pts',(141.297487376632,0.204792950453107,339.915705444923));
#41246=CARTESIAN_POINT('Ctrl Pts',(141.290075572455,0.334557475968693,339.906857890522));
#41247=CARTESIAN_POINT('Ctrl Pts',(141.282300493676,0.470682147428127,339.897576691123));
#41248=CARTESIAN_POINT('Ctrl Pts',(141.274525414898,0.606635414813306,339.882612035073));
#41249=CARTESIAN_POINT('Ctrl Pts',(141.26675033612,0.741904377521809,339.861970892253));
#41250=CARTESIAN_POINT('Ctrl Pts',(141.258984825071,0.877006883160056,339.841355149673));
#41251=CARTESIAN_POINT('Ctrl Pts',(141.251219314022,1.01142637691261,339.815076877422));
#41252=CARTESIAN_POINT('Ctrl Pts',(141.243453802973,1.14465225260247,339.783194986943));
#41253=CARTESIAN_POINT('Ctrl Pts',(141.23569599145,1.2777460344488,339.751344707451));
#41254=CARTESIAN_POINT('Ctrl Pts',(141.227938179928,1.40964817572406,339.713901956877));
#41255=CARTESIAN_POINT('Ctrl Pts',(141.220180368406,1.53985582811249,339.670977102398));
#41256=CARTESIAN_POINT('Ctrl Pts',(141.212428394883,1.66996549511275,339.628084550234));
#41257=CARTESIAN_POINT('Ctrl Pts',(141.20467642136,1.79838284163539,339.57971822757));
#41258=CARTESIAN_POINT('Ctrl Pts',(141.196924447837,1.92461815748993,339.526038887411));
#41259=CARTESIAN_POINT('Ctrl Pts',(141.189175757279,2.05080001261378,339.472382280485));
#41260=CARTESIAN_POINT('Ctrl Pts',(141.181427066722,2.17480131606695,339.413417283924));
#41261=CARTESIAN_POINT('Ctrl Pts',(141.173678376164,2.29615060367084,339.349353453993));
#41262=CARTESIAN_POINT('Ctrl Pts',(141.165931297786,2.41747464354182,339.285302953077));
#41263=CARTESIAN_POINT('Ctrl Pts',(141.158184219408,2.53614741963648,339.216155911276));
#41264=CARTESIAN_POINT('Ctrl Pts',(141.150437141031,2.651720788228,339.142168504996));
#41265=CARTESIAN_POINT('Ctrl Pts',(141.142689997725,2.7672951254357,339.06818047863));
#41266=CARTESIAN_POINT('Ctrl Pts',(141.134942854419,2.87976967413334,338.989352217615));
#41267=CARTESIAN_POINT('Ctrl Pts',(141.127195711113,2.98872441753231,338.905983796503));
#41268=CARTESIAN_POINT('Ctrl Pts',(141.119446826085,3.0977036562707,338.822596632401));
#41269=CARTESIAN_POINT('Ctrl Pts',(141.111697941057,3.20316120469366,338.734667514554));
#41270=CARTESIAN_POINT('Ctrl Pts',(141.103949056029,3.30470965500933,338.642537186988));
#41271=CARTESIAN_POINT('Ctrl Pts',(141.096191946254,3.40636588989946,338.55030907134));
#41272=CARTESIAN_POINT('Ctrl Pts',(141.088434836479,3.5041044484065,338.453871101341));
#41273=CARTESIAN_POINT('Ctrl Pts',(141.080677726705,3.5975739951362,338.353601707421));
#41274=CARTESIAN_POINT('Ctrl Pts',(141.072916471778,3.69109348900298,338.253278732743));
#41275=CARTESIAN_POINT('Ctrl Pts',(141.065155216852,3.78033917135454,338.149120551204));
#41276=CARTESIAN_POINT('Ctrl Pts',(141.057393961926,3.86500031053346,338.041538370969));
#41277=CARTESIAN_POINT('Ctrl Pts',(141.049620291521,3.94979687994415,337.933784094307));
#41278=CARTESIAN_POINT('Ctrl Pts',(141.041846621117,4.02999402235305,337.822595190901));
#41279=CARTESIAN_POINT('Ctrl Pts',(141.034072950712,4.10532412499918,337.708412245431));
#41280=CARTESIAN_POINT('Ctrl Pts',(141.026661146535,4.17714759324341,337.599544543543));
#41281=CARTESIAN_POINT('Ctrl Pts',(141.019249342358,4.24454679711922,337.487955518265));
#41282=CARTESIAN_POINT('Ctrl Pts',(141.011837538181,4.30732973051173,337.374045840996));
#41283=CARTESIAN_POINT('Ctrl Pts',(141.004062459403,4.37318984249072,337.254553111124));
#41284=CARTESIAN_POINT('Ctrl Pts',(140.996287380624,4.43417785794029,337.132128874084));
#41285=CARTESIAN_POINT('Ctrl Pts',(140.988512301846,4.49002207803601,337.007208210737));
#41286=CARTESIAN_POINT('Ctrl Pts',(140.980746790797,4.5457975782636,336.882441270219));
#41287=CARTESIAN_POINT('Ctrl Pts',(140.972981279748,4.59644171956362,336.755184369247));
#41288=CARTESIAN_POINT('Ctrl Pts',(140.965215768699,4.6417277235244,336.62589876781));
#41289=CARTESIAN_POINT('Ctrl Pts',(140.957457957177,4.68696882628041,336.496741353423));
#41290=CARTESIAN_POINT('Ctrl Pts',(140.949700145654,4.7268622357043,336.365559608016));
#41291=CARTESIAN_POINT('Ctrl Pts',(140.941942334132,4.7612286418322,336.232836113478));
#41292=CARTESIAN_POINT('Ctrl Pts',(140.934190360609,4.7955691861499,336.100212497579));
#41293=CARTESIAN_POINT('Ctrl Pts',(140.926438387086,4.82439090836163,335.966049818771));
#41294=CARTESIAN_POINT('Ctrl Pts',(140.918686413563,4.84756397881346,335.830846877475));
#41295=CARTESIAN_POINT('Ctrl Pts',(140.910937723005,4.87072723545608,335.695701194706));
#41296=CARTESIAN_POINT('Ctrl Pts',(140.903189032448,4.88824653237722,335.559516510131));
#41297=CARTESIAN_POINT('Ctrl Pts',(140.89544034189,4.90004295358947,335.422802690954));
#41298=CARTESIAN_POINT('Ctrl Pts',(140.887693263512,4.91183692045776,335.286117316229));
#41299=CARTESIAN_POINT('Ctrl Pts',(140.879946185135,4.9179103464071,335.148903415064));
#41300=CARTESIAN_POINT('Ctrl Pts',(140.872199106757,4.91823613935751,335.011676472831));
#41301=CARTESIAN_POINT('Ctrl Pts',(140.864451963451,4.91856193503837,334.874448380504));
#41302=CARTESIAN_POINT('Ctrl Pts',(140.856704820145,4.91314000071226,334.737207637765));
#41303=CARTESIAN_POINT('Ctrl Pts',(140.848957676839,4.90199538028729,334.600469833252));
#41304=CARTESIAN_POINT('Ctrl Pts',(140.841208791811,4.89084825431497,334.463701287175));
#41305=CARTESIAN_POINT('Ctrl Pts',(140.833459906783,4.87397591383677,334.327436293829));
#41306=CARTESIAN_POINT('Ctrl Pts',(140.825711021755,4.85145524918657,334.192185028834));
#41307=CARTESIAN_POINT('Ctrl Pts',(140.81795391198,4.82891068087031,334.056790206749));
#41308=CARTESIAN_POINT('Ctrl Pts',(140.810196802205,4.80070587673029,333.922411648564));
#41309=CARTESIAN_POINT('Ctrl Pts',(140.802439692431,4.7669689392463,333.789549590127));
#41310=CARTESIAN_POINT('Ctrl Pts',(140.794678437505,4.73321397382166,333.656616534455));
#41311=CARTESIAN_POINT('Ctrl Pts',(140.786917182578,4.69392109648418,333.525201967566));
#41312=CARTESIAN_POINT('Ctrl Pts',(140.779155927652,4.64926794622451,333.395789718675));
#41313=CARTESIAN_POINT('Ctrl Pts',(140.771382257248,4.60454336547684,333.266170452361));
#41314=CARTESIAN_POINT('Ctrl Pts',(140.763608586843,4.55444151996085,333.138560268728));
#41315=CARTESIAN_POINT('Ctrl Pts',(140.755834916438,4.49918808611068,333.013422634706));
#41316=CARTESIAN_POINT('Ctrl Pts',(140.748423112261,4.44650671289935,332.894110187653));
#41317=CARTESIAN_POINT('Ctrl Pts',(140.741011308084,4.38914269747793,332.77704553466));
#41318=CARTESIAN_POINT('Ctrl Pts',(140.733599503907,4.32732906744816,332.662606964048));
#41319=CARTESIAN_POINT('Ctrl Pts',(140.725824425129,4.26248576727736,332.542559418195));
#41320=CARTESIAN_POINT('Ctrl Pts',(140.71804934635,4.19254072919499,332.425022515518));
#41321=CARTESIAN_POINT('Ctrl Pts',(140.710274267572,4.11771279015552,332.310460180572));
#41322=CARTESIAN_POINT('Ctrl Pts',(140.702508756523,4.04297693165904,332.196038821873));
#41323=CARTESIAN_POINT('Ctrl Pts',(140.694743245474,3.9633703395422,332.084585071893));
#41324=CARTESIAN_POINT('Ctrl Pts',(140.686977734425,3.87915817435981,331.976539247684));
#41325=CARTESIAN_POINT('Ctrl Pts',(140.679219922903,3.79502950578445,331.868600551224));
#41326=CARTESIAN_POINT('Ctrl Pts',(140.67146211138,3.706304590355,331.764063362504));
#41327=CARTESIAN_POINT('Ctrl Pts',(140.663704299858,3.61329220656668,331.66333961985));
#41328=CARTESIAN_POINT('Ctrl Pts',(140.655952326335,3.52034981754666,331.562691675005));
#41329=CARTESIAN_POINT('Ctrl Pts',(140.648200352812,3.42312664638137,331.465851750158));
#41330=CARTESIAN_POINT('Ctrl Pts',(140.640448379289,3.32197188671056,331.373198951362));
#41331=CARTESIAN_POINT('Ctrl Pts',(140.632699688732,3.22085996614025,331.28058539108));
#41332=CARTESIAN_POINT('Ctrl Pts',(140.624950998174,3.11582005632932,331.192155693442));
#41333=CARTESIAN_POINT('Ctrl Pts',(140.617202307616,3.00723820951844,331.108252138985));
#41334=CARTESIAN_POINT('Ctrl Pts',(140.609455229239,2.89867895406761,331.024366041364));
#41335=CARTESIAN_POINT('Ctrl Pts',(140.601708150861,2.78657953652146,330.945004452659));
#41336=CARTESIAN_POINT('Ctrl Pts',(140.593961072483,2.67135877844877,330.870469113894));
#41337=CARTESIAN_POINT('Ctrl Pts',(140.586213929177,2.55613705471535,330.795933150451));
#41338=CARTESIAN_POINT('Ctrl Pts',(140.578466785871,2.43779426646905,330.726223729929));
#41339=CARTESIAN_POINT('Ctrl Pts',(140.570719642565,2.31677753588989,330.661598806969));
#41340=CARTESIAN_POINT('Ctrl Pts',(140.562970757537,2.1957335981806,330.596959354953));
#41341=CARTESIAN_POINT('Ctrl Pts',(140.555221872509,2.07201486662305,330.537406859234));
#41342=CARTESIAN_POINT('Ctrl Pts',(140.547472987481,1.94609196855235,330.483152746391));
#41343=CARTESIAN_POINT('Ctrl Pts',(140.539715877706,1.82003541461648,330.428841047672));
#41344=CARTESIAN_POINT('Ctrl Pts',(140.531958767932,1.69177038028666,330.379839120722));
#41345=CARTESIAN_POINT('Ctrl Pts',(140.524201658157,1.56178684816186,330.336309947755));
#41346=CARTESIAN_POINT('Ctrl Pts',(140.516440403231,1.43173385699337,330.292757514189));
#41347=CARTESIAN_POINT('Ctrl Pts',(140.508679148305,1.29996091353737,330.254683770309));
#41348=CARTESIAN_POINT('Ctrl Pts',(140.500917893378,1.16697101075282,330.222201163447));
#41349=CARTESIAN_POINT('Ctrl Pts',(140.493144222974,1.03376836746512,330.189666595001));
#41350=CARTESIAN_POINT('Ctrl Pts',(140.485370552569,0.899345258152152,330.162741113136));
#41351=CARTESIAN_POINT('Ctrl Pts',(140.477596882164,0.764213548510509,330.141485750276));
#41352=CARTESIAN_POINT('Ctrl Pts',(140.470185077987,0.635372252462299,330.12121982967));
#41353=CARTESIAN_POINT('Ctrl Pts',(140.46277327381,0.505887128002858,330.106108053142));
#41354=CARTESIAN_POINT('Ctrl Pts',(140.455361469633,0.37620239045995,330.096159176328));
#41355=CARTESIAN_POINT('Ctrl Pts',(140.447586390855,0.240161417620565,330.085722675425));
#41356=CARTESIAN_POINT('Ctrl Pts',(140.439811312076,0.10347085506739,330.080934987856));
#41357=CARTESIAN_POINT('Ctrl Pts',(140.432036233298,-0.0333607479093066,
330.081863145154));
#41358=CARTESIAN_POINT('Ctrl Pts',(140.424270722249,-0.170023970887461,
330.082790160295));
#41359=CARTESIAN_POINT('Ctrl Pts',(140.4165052112,-0.306827501827269,330.089419022609));
#41360=CARTESIAN_POINT('Ctrl Pts',(140.408739700151,-0.443257575134837,
330.101765033751));
#41361=CARTESIAN_POINT('Ctrl Pts',(140.400981888628,-0.579552377627468,
330.114098803787));
#41362=CARTESIAN_POINT('Ctrl Pts',(140.393224077106,-0.715474072598671,
330.132138406876));
#41363=CARTESIAN_POINT('Ctrl Pts',(140.385466265584,-0.850509154561626,
330.155847108058));
#41364=CARTESIAN_POINT('Ctrl Pts',(140.377714292061,-0.985442618342828,
330.179537967691));
#41365=CARTESIAN_POINT('Ctrl Pts',(140.369962318538,-1.11949041371819,330.208889366481));
#41366=CARTESIAN_POINT('Ctrl Pts',(140.362210345015,-1.25214477360342,330.243812816085));
#41367=CARTESIAN_POINT('Ctrl Pts',(140.354461654457,-1.38474295428892,330.278721475588));
#41368=CARTESIAN_POINT('Ctrl Pts',(140.3467129639,-1.51594849598507,330.319197393189));
#41369=CARTESIAN_POINT('Ctrl Pts',(140.338964273342,-1.64526465266629,330.365101156963));
#41370=CARTESIAN_POINT('Ctrl Pts',(140.331217194964,-1.77455390404073,330.410995370075));
#41371=CARTESIAN_POINT('Ctrl Pts',(140.323470116586,-1.90195418418469,330.462315052411));
#41372=CARTESIAN_POINT('Ctrl Pts',(140.315723038209,-2.02698510425249,330.518871297358));
#41373=CARTESIAN_POINT('Ctrl Pts',(140.307975894903,-2.15201707220025,330.575428016302));
#41374=CARTESIAN_POINT('Ctrl Pts',(140.300228751597,-2.27467928433013,330.637221224301));
#41375=CARTESIAN_POINT('Ctrl Pts',(140.292481608291,-2.3945128576153,330.704014520833));
#41376=CARTESIAN_POINT('Ctrl Pts',(140.284732723263,-2.51437337203151,330.770822833915));
#41377=CARTESIAN_POINT('Ctrl Pts',(140.276983838235,-2.63140364080378,330.84263328215));
#41378=CARTESIAN_POINT('Ctrl Pts',(140.269234953207,-2.74517118735471,330.919164520026));
#41379=CARTESIAN_POINT('Ctrl Pts',(140.261477843432,-2.85905948795526,330.995776988948));
#41380=CARTESIAN_POINT('Ctrl Pts',(140.253720733657,-2.9696778236595,331.077120038328));
#41381=CARTESIAN_POINT('Ctrl Pts',(140.245963623883,-3.07662398154829,331.162869830373));
#41382=CARTESIAN_POINT('Ctrl Pts',(140.238202368957,-3.18362728804423,331.248665444365));
#41383=CARTESIAN_POINT('Ctrl Pts',(140.23044111403,-3.28695421237456,331.338872236285));
#41384=CARTESIAN_POINT('Ctrl Pts',(140.222679859104,-3.38623799682626,331.433128080327));
#41385=CARTESIAN_POINT('Ctrl Pts',(140.2149061887,-3.48568060297654,331.527534703002));
#41386=CARTESIAN_POINT('Ctrl Pts',(140.207132518295,-3.5810668727517,331.626003040194));
#41387=CARTESIAN_POINT('Ctrl Pts',(140.19935884789,-3.67206848278731,331.728135681264));
#41388=CARTESIAN_POINT('Ctrl Pts',(140.191947043713,-3.75883394598241,331.82551402332));
#41389=CARTESIAN_POINT('Ctrl Pts',(140.184535239536,-3.84161359195973,331.926222977529));
#41390=CARTESIAN_POINT('Ctrl Pts',(140.177123435359,-3.9201596675152,332.02989373192));
#41391=CARTESIAN_POINT('Ctrl Pts',(140.169326540512,-4.00278671446171,332.138950845589));
#41392=CARTESIAN_POINT('Ctrl Pts',(140.161529645666,-4.0809922521438,332.25163379844));
#41393=CARTESIAN_POINT('Ctrl Pts',(140.15373275082,-4.15444223853103,332.367550048109));
#41394=CARTESIAN_POINT('Ctrl Pts',(140.145945417238,-4.22780215383955,332.483324150692));
#41395=CARTESIAN_POINT('Ctrl Pts',(140.138158083656,-4.29641791378443,332.602323338621));
#41396=CARTESIAN_POINT('Ctrl Pts',(140.130370750073,-4.3599959443122,332.724122492734));
#41397=CARTESIAN_POINT('Ctrl Pts',(140.122591313883,-4.42350949825989,332.845798126302));
#41398=CARTESIAN_POINT('Ctrl Pts',(140.114811877693,-4.48199531007374,332.970267735069));
#41399=CARTESIAN_POINT('Ctrl Pts',(140.107032441503,-4.5352035263831,333.097078026617));
#41400=CARTESIAN_POINT('Ctrl Pts',(140.0992592446,-4.58836906848031,333.223786613398));
#41401=CARTESIAN_POINT('Ctrl Pts',(140.091486047697,-4.63626528978345,333.352831791015));
#41402=CARTESIAN_POINT('Ctrl Pts',(140.083712850793,-4.67868881687082,333.483736824496));
#41403=CARTESIAN_POINT('Ctrl Pts',(140.075944143033,-4.72108784370571,333.614566258267));
#41404=CARTESIAN_POINT('Ctrl Pts',(140.068175435273,-4.75802034867188,333.747253041976));
#41405=CARTESIAN_POINT('Ctrl Pts',(140.060406727513,-4.78933166584142,333.881301981289));
#41406=CARTESIAN_POINT('Ctrl Pts',(140.052640748718,-4.82063198407799,334.015303832346));
#41407=CARTESIAN_POINT('Ctrl Pts',(140.044874769923,-4.84631495845551,334.150666509196));
#41408=CARTESIAN_POINT('Ctrl Pts',(140.037108791128,-4.86627631122856,334.286881548916));
#41409=CARTESIAN_POINT('Ctrl Pts',(140.029342347225,-4.88623885949439,334.423104746606));
#41410=CARTESIAN_POINT('Ctrl Pts',(140.021575903323,-4.9004790384385,334.560180026654));
#41411=CARTESIAN_POINT('Ctrl Pts',(140.013809459421,-4.90894404984525,334.69759071114));
#41412=CARTESIAN_POINT('Ctrl Pts',(140.008051722444,-4.91521967737826,334.799461604568));
#41413=CARTESIAN_POINT('Ctrl Pts',(140.002293985467,-4.91832224859098,334.901516643467));
#41414=CARTESIAN_POINT('Ctrl Pts',(139.99653624849,-4.91824872290653,335.003544309289));
#41415=CARTESIAN_POINT('',(143.496536248456,-4.91824957381542,334.997952522408));
#41416=CARTESIAN_POINT('Ctrl Pts',(143.496536248456,-4.91824957381541,334.997952522409));
#41417=CARTESIAN_POINT('Ctrl Pts',(143.488840527635,-4.91830583800652,335.133104836198));
#41418=CARTESIAN_POINT('Ctrl Pts',(143.481144806814,-4.9127869647833,335.268484246378));
#41419=CARTESIAN_POINT('Ctrl Pts',(143.473449085993,-4.90166304579241,335.403586977011));
#41420=CARTESIAN_POINT('Ctrl Pts',(143.465762407207,-4.89055219677536,335.538530969599));
#41421=CARTESIAN_POINT('Ctrl Pts',(143.458075728422,-4.87384943324171,335.673198534926));
#41422=CARTESIAN_POINT('Ctrl Pts',(143.450389049636,-4.85157683415553,335.807084434731));
#41423=CARTESIAN_POINT('Ctrl Pts',(143.442709473782,-4.82932481622644,335.940846616298));
#41424=CARTESIAN_POINT('Ctrl Pts',(143.435029897928,-4.80151326699133,336.073828177672));
#41425=CARTESIAN_POINT('Ctrl Pts',(143.427350322074,-4.76821615087756,336.205528017514));
#41426=CARTESIAN_POINT('Ctrl Pts',(143.419449967503,-4.73396178208414,336.341014071878));
#41427=CARTESIAN_POINT('Ctrl Pts',(143.411549612932,-4.69390170447446,336.475143167105));
#41428=CARTESIAN_POINT('Ctrl Pts',(143.403649258361,-4.6481732473492,336.60737939676));
#41429=CARTESIAN_POINT('Ctrl Pts',(143.395977266379,-4.60376658771376,336.735793290665));
#41430=CARTESIAN_POINT('Ctrl Pts',(143.388305274396,-4.55401486860619,336.862421837089));
#41431=CARTESIAN_POINT('Ctrl Pts',(143.380633282414,-4.49909457980441,336.986789124309));
#41432=CARTESIAN_POINT('Ctrl Pts',(143.372962119359,-4.44418022491634,337.111142974151));
#41433=CARTESIAN_POINT('Ctrl Pts',(143.365290956305,-4.38409857211948,337.233235685312));
#41434=CARTESIAN_POINT('Ctrl Pts',(143.35761979325,-4.31907404683682,337.35261183378));
#41435=CARTESIAN_POINT('Ctrl Pts',(143.349947717993,-4.25404178928833,337.472002177632));
#41436=CARTESIAN_POINT('Ctrl Pts',(143.342275642737,-4.18406568151538,337.58867496567));
#41437=CARTESIAN_POINT('Ctrl Pts',(143.334603567481,-4.10941558937893,337.70220032127));
#41438=CARTESIAN_POINT('Ctrl Pts',(143.326531754555,-4.03087600804304,337.821640681551));
#41439=CARTESIAN_POINT('Ctrl Pts',(143.318459941629,-3.9471625706808,337.937596400006));
#41440=CARTESIAN_POINT('Ctrl Pts',(143.310388128704,-3.85863976017585,338.049603624029));
#41441=CARTESIAN_POINT('Ctrl Pts',(143.302704741091,-3.774376773414,338.156220926182));
#41442=CARTESIAN_POINT('Ctrl Pts',(143.295021353478,-3.68575677496038,338.259260601928));
#41443=CARTESIAN_POINT('Ctrl Pts',(143.287337965865,-3.59313334160412,338.358359101102));
#41444=CARTESIAN_POINT('Ctrl Pts',(143.27964941016,-3.50044760677403,338.457524257085));
#41445=CARTESIAN_POINT('Ctrl Pts',(143.271960854456,-3.40375335973002,338.552742679942));
#41446=CARTESIAN_POINT('Ctrl Pts',(143.264272298752,-3.30343869949283,338.643689863475));
#41447=CARTESIAN_POINT('Ctrl Pts',(143.256573199342,-3.20298647268547,338.734761767485));
#41448=CARTESIAN_POINT('Ctrl Pts',(143.248874099932,-3.09890423223411,338.82155049195));
#41449=CARTESIAN_POINT('Ctrl Pts',(143.241175000522,-2.99161071287561,338.903773610893));
#41450=CARTESIAN_POINT('Ctrl Pts',(143.240030604472,-2.97566257749354,338.915995275727));
#41451=CARTESIAN_POINT('Ctrl Pts',(143.238886208422,-2.95964353913426,338.928116149807));
#41452=CARTESIAN_POINT('Ctrl Pts',(143.237741812373,-2.94355502036444,338.940135391657));
#41453=CARTESIAN_POINT('Ctrl Pts',(143.229966733594,-2.834248892561,339.021794667106));
#41454=CARTESIAN_POINT('Ctrl Pts',(143.222191654816,-2.72136941230709,339.099031023707));
#41455=CARTESIAN_POINT('Ctrl Pts',(143.214416576037,-2.6053101860245,339.171515539597));
#41456=CARTESIAN_POINT('Ctrl Pts',(143.206651064988,-2.48939377800862,339.243910858676));
#41457=CARTESIAN_POINT('Ctrl Pts',(143.198885553939,-2.370305737832,339.311565766702));
#41458=CARTESIAN_POINT('Ctrl Pts',(143.19112004289,-2.24847177687613,339.374192237556));
#41459=CARTESIAN_POINT('Ctrl Pts',(143.183362231368,-2.12675861464739,339.436756614081));
#41460=CARTESIAN_POINT('Ctrl Pts',(143.175604419846,-2.00230529514067,339.494302297735));
#41461=CARTESIAN_POINT('Ctrl Pts',(143.167846608324,-1.87556517379614,339.546585349616));
#41462=CARTESIAN_POINT('Ctrl Pts',(143.160094634801,-1.74892042841222,339.598829056843));
#41463=CARTESIAN_POINT('Ctrl Pts',(143.152342661278,-1.6199926664213,339.645817866616));
#41464=CARTESIAN_POINT('Ctrl Pts',(143.144590687755,-1.48925810892312,339.68735462148));
#41465=CARTESIAN_POINT('Ctrl Pts',(143.136841997197,-1.3585789175874,339.728873785503));
#41466=CARTESIAN_POINT('Ctrl Pts',(143.12909330664,-1.22609482438024,339.764945368841));
#41467=CARTESIAN_POINT('Ctrl Pts',(143.121344616082,-1.09230001022392,339.795421123339));
#41468=CARTESIAN_POINT('Ctrl Pts',(143.113597537704,-0.958533033196216,
339.825890537102));
#41469=CARTESIAN_POINT('Ctrl Pts',(143.105850459327,-0.823456258525038,
339.850766351064));
#41470=CARTESIAN_POINT('Ctrl Pts',(143.098103380949,-0.687576555167322,
339.869950876886));
#41471=CARTESIAN_POINT('Ctrl Pts',(143.090356237643,-0.551695713006862,
339.889135563493));
#41472=CARTESIAN_POINT('Ctrl Pts',(143.082609094337,-0.41501231577349,339.902628812179));
#41473=CARTESIAN_POINT('Ctrl Pts',(143.074861951031,-0.278040500792239,
339.910384561561));
#41474=CARTESIAN_POINT('Ctrl Pts',(143.067113066003,-0.141037891639126,
339.918142054601));
#41475=CARTESIAN_POINT('Ctrl Pts',(143.059364180975,-0.00374712588186016,
339.920159459465));
#41476=CARTESIAN_POINT('Ctrl Pts',(143.051615295947,0.133315894509946,339.916442813129));
#41477=CARTESIAN_POINT('Ctrl Pts',(143.043858186172,0.270524395008002,339.912722221906));
#41478=CARTESIAN_POINT('Ctrl Pts',(143.036101076398,0.407504275911864,339.903255432377));
#41479=CARTESIAN_POINT('Ctrl Pts',(143.028343966623,0.5437424415808,339.888100573814));
#41480=CARTESIAN_POINT('Ctrl Pts',(143.020582711697,0.680053408569185,339.87293761698));
#41481=CARTESIAN_POINT('Ctrl Pts',(143.012821456771,0.815621484428806,339.852080593996));
#41482=CARTESIAN_POINT('Ctrl Pts',(143.005060201844,0.949943015645992,339.825638955571));
#41483=CARTESIAN_POINT('Ctrl Pts',(142.99728653144,1.08447941753802,339.799155019142));
#41484=CARTESIAN_POINT('Ctrl Pts',(142.989512861035,1.21776490983714,339.767068706896));
#41485=CARTESIAN_POINT('Ctrl Pts',(142.98173919063,1.34930940530986,339.729539849842));
#41486=CARTESIAN_POINT('Ctrl Pts',(142.974327386453,1.47473047287291,339.693757970112));
#41487=CARTESIAN_POINT('Ctrl Pts',(142.966915582276,1.59856870936171,339.653028933421));
#41488=CARTESIAN_POINT('Ctrl Pts',(142.959503778099,1.72041738727867,339.607531559962));
#41489=CARTESIAN_POINT('Ctrl Pts',(142.95172869932,1.84823823186638,339.559804224702));
#41490=CARTESIAN_POINT('Ctrl Pts',(142.943953620542,1.97427349568604,339.506678485956));
#41491=CARTESIAN_POINT('Ctrl Pts',(142.936178541763,2.09803357830588,339.448307337269));
#41492=CARTESIAN_POINT('Ctrl Pts',(142.928413030714,2.2216413662652,339.390008017996));
#41493=CARTESIAN_POINT('Ctrl Pts',(142.920647519665,2.3429791935886,339.32647629715));
#41494=CARTESIAN_POINT('Ctrl Pts',(142.912882008616,2.46157447611125,339.257914297054));
#41495=CARTESIAN_POINT('Ctrl Pts',(142.905124197094,2.58005217106592,339.18942027638));
#41496=CARTESIAN_POINT('Ctrl Pts',(142.897366385572,2.69579239644874,339.115906096308));
#41497=CARTESIAN_POINT('Ctrl Pts',(142.88960857405,2.80834468219192,339.037620983761));
#41498=CARTESIAN_POINT('Ctrl Pts',(142.881856600527,2.92081226877096,338.959394783243));
#41499=CARTESIAN_POINT('Ctrl Pts',(142.874104627004,3.03009637125878,338.876405018817));
#41500=CARTESIAN_POINT('Ctrl Pts',(142.866352653481,3.13577348518116,338.788945461753));
#41501=CARTESIAN_POINT('Ctrl Pts',(142.858603962923,3.24140584478293,338.701522943862));
#41502=CARTESIAN_POINT('Ctrl Pts',(142.850855272365,3.3434339535351,338.609634646991));
#41503=CARTESIAN_POINT('Ctrl Pts',(142.843106581808,3.44146571674916,338.513615912837));
#41504=CARTESIAN_POINT('Ctrl Pts',(142.83535950343,3.53947708363611,338.417617156183));
#41505=CARTESIAN_POINT('Ctrl Pts',(142.827612425052,3.633493479777,338.317489944933));
#41506=CARTESIAN_POINT('Ctrl Pts',(142.819865346674,3.72315846108758,338.213607651244));
#41507=CARTESIAN_POINT('Ctrl Pts',(142.812118203368,3.81282419387709,338.10972448692));
#41508=CARTESIAN_POINT('Ctrl Pts',(142.804371060062,3.89813818369696,338.00208647328));
#41509=CARTESIAN_POINT('Ctrl Pts',(142.796623916757,3.97878346734188,337.891101032912));
#41510=CARTESIAN_POINT('Ctrl Pts',(142.788875031728,4.05944688175883,337.780090640661));
#41511=CARTESIAN_POINT('Ctrl Pts',(142.7811261467,4.13543927164257,337.665731640296));
#41512=CARTESIAN_POINT('Ctrl Pts',(142.773377261672,4.20648652945596,337.548461131743));
#41513=CARTESIAN_POINT('Ctrl Pts',(142.765620151897,4.27760919756266,337.431066151061));
#41514=CARTESIAN_POINT('Ctrl Pts',(142.757863042123,4.34377604574314,337.310753823853));
#41515=CARTESIAN_POINT('Ctrl Pts',(142.750105932348,4.4047582906504,337.187987080274));
#41516=CARTESIAN_POINT('Ctrl Pts',(142.742344677422,4.46577312251947,337.065154734073));
#41517=CARTESIAN_POINT('Ctrl Pts',(142.734583422496,4.52159767166923,336.939865714952));
#41518=CARTESIAN_POINT('Ctrl Pts',(142.726822167569,4.57205142171969,336.812602785955));
#41519=CARTESIAN_POINT('Ctrl Pts',(142.719048497165,4.62258588132743,336.685136277746));
#41520=CARTESIAN_POINT('Ctrl Pts',(142.71127482676,4.6677322446311,336.555689919082));
#41521=CARTESIAN_POINT('Ctrl Pts',(142.703501156355,4.70735970261259,336.424762328502));
#41522=CARTESIAN_POINT('Ctrl Pts',(142.696089352178,4.74514249289104,336.299929448764));
#41523=CARTESIAN_POINT('Ctrl Pts',(142.688677548001,4.77790855262165,336.173750414946));
#41524=CARTESIAN_POINT('Ctrl Pts',(142.681265743824,4.80558815193244,336.046664022744));
#41525=CARTESIAN_POINT('Ctrl Pts',(142.673490665046,4.83462441085886,335.913348747889));
#41526=CARTESIAN_POINT('Ctrl Pts',(142.665715586267,4.85815475691442,335.778613620109));
#41527=CARTESIAN_POINT('Ctrl Pts',(142.657940507489,4.87604289474714,335.642953148438));
#41528=CARTESIAN_POINT('Ctrl Pts',(142.65017499644,4.89390902008739,335.507459615614));
#41529=CARTESIAN_POINT('Ctrl Pts',(142.642409485391,4.90614670136614,335.37104338839));
#41530=CARTESIAN_POINT('Ctrl Pts',(142.634643974342,4.9126701651479,335.234211252859));
#41531=CARTESIAN_POINT('Ctrl Pts',(142.62688616282,4.91918716089635,335.097514786788));
#41532=CARTESIAN_POINT('Ctrl Pts',(142.619128351298,4.92000119564422,334.960403620974));
#41533=CARTESIAN_POINT('Ctrl Pts',(142.611370539776,4.91507807442839,334.823391436297));
#41534=CARTESIAN_POINT('Ctrl Pts',(142.603618566252,4.91015865801739,334.686482357633));
#41535=CARTESIAN_POINT('Ctrl Pts',(142.595866592729,4.8995106931793,334.549672500894));
#41536=CARTESIAN_POINT('Ctrl Pts',(142.588114619206,4.88315203587047,334.413476976518));
#41537=CARTESIAN_POINT('Ctrl Pts',(142.580365928649,4.86680030646277,334.277339131028));
#41538=CARTESIAN_POINT('Ctrl Pts',(142.572617238091,4.84474274129044,334.141815487718));
#41539=CARTESIAN_POINT('Ctrl Pts',(142.564868547534,4.81704915140712,334.007417240011));
#41540=CARTESIAN_POINT('Ctrl Pts',(142.557121469156,4.78936132340645,333.873046954981));
#41541=CARTESIAN_POINT('Ctrl Pts',(142.549374390778,4.75603988195816,333.739801982409));
#41542=CARTESIAN_POINT('Ctrl Pts',(142.5416273124,4.71720591132571,333.608184116827));
#41543=CARTESIAN_POINT('Ctrl Pts',(142.533880169094,4.67837161522723,333.476565148159));
#41544=CARTESIAN_POINT('Ctrl Pts',(142.526133025789,4.63402480840819,333.346573688577));
#41545=CARTESIAN_POINT('Ctrl Pts',(142.518385882483,4.58433657423815,333.218696758942));
#41546=CARTESIAN_POINT('Ctrl Pts',(142.510636997455,4.53463716909814,333.090791079859));
#41547=CARTESIAN_POINT('Ctrl Pts',(142.502888112427,4.47959408855751,332.965001240964));
#41548=CARTESIAN_POINT('Ctrl Pts',(142.495139227399,4.4194265639526,332.841794284983));
#41549=CARTESIAN_POINT('Ctrl Pts',(142.487382117624,4.35919517691543,332.718456555867));
#41550=CARTESIAN_POINT('Ctrl Pts',(142.479625007849,4.29382865241851,332.597707537852));
#41551=CARTESIAN_POINT('Ctrl Pts',(142.471867898074,4.22359247050929,332.479990137806));
#41552=CARTESIAN_POINT('Ctrl Pts',(142.464106643148,4.15331875663018,332.362209833344));
#41553=CARTESIAN_POINT('Ctrl Pts',(142.456345388222,4.07817041428427,332.247464701671));
#41554=CARTESIAN_POINT('Ctrl Pts',(142.448584133296,3.99845572144275,332.136167793644));
#41555=CARTESIAN_POINT('Ctrl Pts',(142.440810462891,3.91861351107166,332.024692846836));
#41556=CARTESIAN_POINT('Ctrl Pts',(142.433036792487,3.83419059413541,331.916677454475));
#41557=CARTESIAN_POINT('Ctrl Pts',(142.425263122082,3.74553548133648,331.812501447757));
#41558=CARTESIAN_POINT('Ctrl Pts',(142.417851317905,3.6610072853676,331.713174859216));
#41559=CARTESIAN_POINT('Ctrl Pts',(142.410439513728,3.57263223895412,331.617338465204));
#41560=CARTESIAN_POINT('Ctrl Pts',(142.403027709551,3.48074159992395,331.525288360589));
#41561=CARTESIAN_POINT('Ctrl Pts',(142.395252630772,3.38434712694685,331.428726606143));
#41562=CARTESIAN_POINT('Ctrl Pts',(142.387477551994,3.28377910397054,331.336026527406));
#41563=CARTESIAN_POINT('Ctrl Pts',(142.379702473216,3.1793796169556,331.247570345258));
#41564=CARTESIAN_POINT('Ctrl Pts',(142.371936962167,3.07510860015578,331.159223014074));
#41565=CARTESIAN_POINT('Ctrl Pts',(142.364171451118,2.96701579590837,331.075109438695));
#41566=CARTESIAN_POINT('Ctrl Pts',(142.356405940069,2.855480954523,330.995575998866));
#41567=CARTESIAN_POINT('Ctrl Pts',(142.348648128546,2.74405670025762,330.916121416675));
#41568=CARTESIAN_POINT('Ctrl Pts',(142.340890317024,2.6291975166976,330.84123815823));
#41569=CARTESIAN_POINT('Ctrl Pts',(142.333132505502,2.51131686419744,330.771232961004));
#41570=CARTESIAN_POINT('Ctrl Pts',(142.325380531979,2.39352492062629,330.701280444909));
#41571=CARTESIAN_POINT('Ctrl Pts',(142.317628558456,2.2727163686305,330.636198882077));
#41572=CARTESIAN_POINT('Ctrl Pts',(142.309876584933,2.14933403844941,330.576252012867));
#41573=CARTESIAN_POINT('Ctrl Pts',(142.302127894375,2.02600396075849,330.516330531192));
#41574=CARTESIAN_POINT('Ctrl Pts',(142.294379203818,1.90010262365113,330.461539588583));
#41575=CARTESIAN_POINT('Ctrl Pts',(142.28663051326,1.77209767934956,330.412097115528));
#41576=CARTESIAN_POINT('Ctrl Pts',(142.278883434882,1.64411936754582,330.362664929393));
#41577=CARTESIAN_POINT('Ctrl Pts',(142.271136356505,1.51403868350181,330.318579140135));
#41578=CARTESIAN_POINT('Ctrl Pts',(142.263389278127,1.3823431225873,330.280009475228));
#41579=CARTESIAN_POINT('Ctrl Pts',(142.255642134821,1.25064645793736,330.24143948707));
#41580=CARTESIAN_POINT('Ctrl Pts',(142.247894991515,1.11733526453966,330.208385825334));
#41581=CARTESIAN_POINT('Ctrl Pts',(142.240147848209,0.982911671655583,330.180968177297));
#41582=CARTESIAN_POINT('Ctrl Pts',(142.232398963181,0.848457857494069,330.153544365191));
#41583=CARTESIAN_POINT('Ctrl Pts',(142.224650078153,0.712891529107122,330.131759166265));
#41584=CARTESIAN_POINT('Ctrl Pts',(142.216901193125,0.576724071343072,330.115680967828));
#41585=CARTESIAN_POINT('Ctrl Pts',(142.20914408335,0.440412084032061,330.099585703826));
#41586=CARTESIAN_POINT('Ctrl Pts',(142.201386973576,0.303498081580096,330.089209586584));
#41587=CARTESIAN_POINT('Ctrl Pts',(142.193629863801,0.166498180307998,330.084569050586));
#41588=CARTESIAN_POINT('Ctrl Pts',(142.185868608875,0.0294250706691604,
330.079926034835));
#41589=CARTESIAN_POINT('Ctrl Pts',(142.178107353948,-0.107733638589367,
330.08102470431));
#41590=CARTESIAN_POINT('Ctrl Pts',(142.170346099022,-0.244463777289203,
330.08782934701));
#41591=CARTESIAN_POINT('Ctrl Pts',(142.162572428618,-0.381412639650758,
330.094644874921));
#41592=CARTESIAN_POINT('Ctrl Pts',(142.154798758213,-0.517931172034827,
330.107184580128));
#41593=CARTESIAN_POINT('Ctrl Pts',(142.147025087808,-0.653511367146012,
330.125360941002));
#41594=CARTESIAN_POINT('Ctrl Pts',(142.139613283631,-0.782780271556707,
330.142691187904));
#41595=CARTESIAN_POINT('Ctrl Pts',(142.132201479454,-0.911195948435113,
330.165145077941));
#41596=CARTESIAN_POINT('Ctrl Pts',(142.124789675277,-1.03833014267276,330.192604283261));
#41597=CARTESIAN_POINT('Ctrl Pts',(142.117014596498,-1.17169556248273,330.221409346031));
#41598=CARTESIAN_POINT('Ctrl Pts',(142.10923951772,-1.30407216418749,330.255813810342));
#41599=CARTESIAN_POINT('Ctrl Pts',(142.101464438941,-1.43495340775072,330.295736850464));
#41600=CARTESIAN_POINT('Ctrl Pts',(142.093698927892,-1.56567359361126,330.335610762743));
#41601=CARTESIAN_POINT('Ctrl Pts',(142.085933416843,-1.69490171237429,330.38098962582));
#41602=CARTESIAN_POINT('Ctrl Pts',(142.078167905794,-1.82214098123911,330.431741545513));
#41603=CARTESIAN_POINT('Ctrl Pts',(142.070410094272,-1.94925409199845,330.482443144531));
#41604=CARTESIAN_POINT('Ctrl Pts',(142.06265228275,-2.07438191643226,330.538507054455));
#41605=CARTESIAN_POINT('Ctrl Pts',(142.054894471228,-2.19704276533312,330.599751580899));
#41606=CARTESIAN_POINT('Ctrl Pts',(142.047142497705,-2.31961130805555,330.660950018896));
#41607=CARTESIAN_POINT('Ctrl Pts',(142.039390524182,-2.43971622217395,330.727321139579));
#41608=CARTESIAN_POINT('Ctrl Pts',(142.031638550659,-2.55689608194047,330.798635282595));
#41609=CARTESIAN_POINT('Ctrl Pts',(142.023889860101,-2.67402631596664,330.869919224029));
#41610=CARTESIAN_POINT('Ctrl Pts',(142.016141169543,-2.78823362624632,330.94614182144));
#41611=CARTESIAN_POINT('Ctrl Pts',(142.008392478986,-2.89908167693048,331.027027750791));
#41612=CARTESIAN_POINT('Ctrl Pts',(142.000645400608,-3.00990666475198,331.107896851148));
#41613=CARTESIAN_POINT('Ctrl Pts',(141.99289832223,-3.11737346763247,331.193427123301));
#41614=CARTESIAN_POINT('Ctrl Pts',(141.985151243852,-3.22107554640128,331.283300471268));
#41615=CARTESIAN_POINT('Ctrl Pts',(141.977404100546,-3.32477849429333,331.37317457246));
#41616=CARTESIAN_POINT('Ctrl Pts',(141.969656957241,-3.42471635975889,331.467391566074));
#41617=CARTESIAN_POINT('Ctrl Pts',(141.961909813935,-3.52051676425655,331.565593970555));
#41618=CARTESIAN_POINT('Ctrl Pts',(141.954160928907,-3.61633870671897,331.663818453022));
#41619=CARTESIAN_POINT('Ctrl Pts',(141.946412043878,-3.70802106434763,331.76602984957));
#41620=CARTESIAN_POINT('Ctrl Pts',(141.93866315885,-3.7952295891095,331.871835134069));
#41621=CARTESIAN_POINT('Ctrl Pts',(141.930906049076,-3.88253067790056,331.977752721389));
#41622=CARTESIAN_POINT('Ctrl Pts',(141.923148939301,-3.96534819910468,332.087271514562));
#41623=CARTESIAN_POINT('Ctrl Pts',(141.915391829526,-4.04338903245736,332.199966394005));
#41624=CARTESIAN_POINT('Ctrl Pts',(141.9076305746,-4.12147156833623,332.312721493987));
#41625=CARTESIAN_POINT('Ctrl Pts',(141.899869319674,-4.19477212148012,332.428655731851));
#41626=CARTESIAN_POINT('Ctrl Pts',(141.892108064748,-4.26304247588702,332.547317405109));
#41627=CARTESIAN_POINT('Ctrl Pts',(141.884334394343,-4.33142204061157,332.666168898372));
#41628=CARTESIAN_POINT('Ctrl Pts',(141.876560723938,-4.39475514628468,332.787756198764));
#41629=CARTESIAN_POINT('Ctrl Pts',(141.868787053534,-4.45284047981482,332.911604749138));
#41630=CARTESIAN_POINT('Ctrl Pts',(141.861375249357,-4.5082219270939,333.029688119694));
#41631=CARTESIAN_POINT('Ctrl Pts',(141.85396344518,-4.55883306317671,333.14982669031));
#41632=CARTESIAN_POINT('Ctrl Pts',(141.846551641003,-4.6045416390662,333.271596298139));
#41633=CARTESIAN_POINT('Ctrl Pts',(141.837634724743,-4.65953223701258,333.418093611081));
#41634=CARTESIAN_POINT('Ctrl Pts',(141.828717808484,-4.70757175041617,333.567334854595));
#41635=CARTESIAN_POINT('Ctrl Pts',(141.819800892224,-4.748414626951,333.718695355094));
#41636=CARTESIAN_POINT('Ctrl Pts',(141.810916116168,-4.78911028909658,333.8695102906));
#41637=CARTESIAN_POINT('Ctrl Pts',(141.802031340113,-4.82266099798843,334.022429090279));
#41638=CARTESIAN_POINT('Ctrl Pts',(141.793146564057,-4.84887039270233,334.176811699989));
#41639=CARTESIAN_POINT('Ctrl Pts',(141.784323191418,-4.87489865213825,334.330127358813));
#41640=CARTESIAN_POINT('Ctrl Pts',(141.775499818779,-4.89368663649289,334.484886506641));
#41641=CARTESIAN_POINT('Ctrl Pts',(141.766676446139,-4.90508935650447,334.64044267883));
#41642=CARTESIAN_POINT('Ctrl Pts',(141.759963046941,-4.91376529194467,334.758799992338));
#41643=CARTESIAN_POINT('Ctrl Pts',(141.753249647743,-4.91816671843185,334.877618301574));
#41644=CARTESIAN_POINT('Ctrl Pts',(141.746536248545,-4.91824882895472,334.996606036901));
#41645=CARTESIAN_POINT('',(145.246536248534,-4.91824795069328,335.004489766291));
#41646=CARTESIAN_POINT('Ctrl Pts',(145.24653624849,-4.91824795069257,335.004489767066));
#41647=CARTESIAN_POINT('Ctrl Pts',(145.235878849129,-4.91807628812392,335.192534951623));
#41648=CARTESIAN_POINT('Ctrl Pts',(145.225221449767,-4.9071165282921,335.380107035918));
#41649=CARTESIAN_POINT('Ctrl Pts',(145.214564050406,-4.88555165495592,335.566187327002));
#41650=CARTESIAN_POINT('Ctrl Pts',(145.204845384367,-4.86588627553186,335.735877149449));
#41651=CARTESIAN_POINT('Ctrl Pts',(145.195126718329,-4.83740238492614,335.904327231285));
#41652=CARTESIAN_POINT('Ctrl Pts',(145.18540805229,-4.80027135218314,336.070783828749));
#41653=CARTESIAN_POINT('Ctrl Pts',(145.177632973512,-4.77056596838255,336.203951606441));
#41654=CARTESIAN_POINT('Ctrl Pts',(145.169857894733,-4.73526799098947,336.336092760649));
#41655=CARTESIAN_POINT('Ctrl Pts',(145.162082815955,-4.69446166592918,336.466701308932));
#41656=CARTESIAN_POINT('Ctrl Pts',(145.154317304906,-4.65370555564978,336.59714913508));
#41657=CARTESIAN_POINT('Ctrl Pts',(145.146551793857,-4.60745470017155,336.726067738318));
#41658=CARTESIAN_POINT('Ctrl Pts',(145.138786282808,-4.55584434678735,336.85296123822));
#41659=CARTESIAN_POINT('Ctrl Pts',(145.131028471285,-4.5042851652188,336.979728922848));
#41660=CARTESIAN_POINT('Ctrl Pts',(145.123270659763,-4.44737720713481,337.104475140226));
#41661=CARTESIAN_POINT('Ctrl Pts',(145.115512848241,-4.38530541692814,337.226719439615));
#41662=CARTESIAN_POINT('Ctrl Pts',(145.107760874718,-4.32328033771178,337.348871746293));
#41663=CARTESIAN_POINT('Ctrl Pts',(145.100008901195,-4.25609933741541,337.468525535432));
#41664=CARTESIAN_POINT('Ctrl Pts',(145.092256927672,-4.18399518841079,337.585220943334));
#41665=CARTESIAN_POINT('Ctrl Pts',(145.084508237114,-4.11192157555631,337.701866930662));
#41666=CARTESIAN_POINT('Ctrl Pts',(145.076759546556,-4.03492916585593,337.815556696807));
#41667=CARTESIAN_POINT('Ctrl Pts',(145.069010855999,-3.95329622482413,337.925855775887));
#41668=CARTESIAN_POINT('Ctrl Pts',(145.061263777621,-3.87168026820744,338.036131906323));
#41669=CARTESIAN_POINT('Ctrl Pts',(145.053516699243,-3.78542593309394,338.143018438918));
#41670=CARTESIAN_POINT('Ctrl Pts',(145.045769620865,-3.69485405466793,338.246110992743));
#41671=CARTESIAN_POINT('Ctrl Pts',(145.038022477559,-3.6042814171625,338.349204410582));
#41672=CARTESIAN_POINT('Ctrl Pts',(145.030275334254,-3.5093914221528,338.448503492585));
#41673=CARTESIAN_POINT('Ctrl Pts',(145.022528190948,-3.41054405871756,338.543638283748));
#41674=CARTESIAN_POINT('Ctrl Pts',(145.01477930592,-3.31167447229633,338.638794463233));
#41675=CARTESIAN_POINT('Ctrl Pts',(145.007030420891,-3.20884602861807,338.729784217906));
#41676=CARTESIAN_POINT('Ctrl Pts',(144.999281535863,-3.10245400292844,338.816275962534));
#41677=CARTESIAN_POINT('Ctrl Pts',(144.991524426089,-2.99594905164362,338.902859510393));
#41678=CARTESIAN_POINT('Ctrl Pts',(144.983767316314,-2.88587326637787,338.984935264271));
#41679=CARTESIAN_POINT('Ctrl Pts',(144.976010206539,-2.77265373724858,339.062212982578));
#41680=CARTESIAN_POINT('Ctrl Pts',(144.968248951613,-2.65937370722299,339.139531995626));
#41681=CARTESIAN_POINT('Ctrl Pts',(144.960487696687,-2.5429469175631,339.212047657725));
#41682=CARTESIAN_POINT('Ctrl Pts',(144.952726441761,-2.42382673732278,339.279514810109));
#41683=CARTESIAN_POINT('Ctrl Pts',(144.944952771356,-2.30451600361524,339.347089887949));
#41684=CARTESIAN_POINT('Ctrl Pts',(144.937179100951,-2.18250361763352,339.409600139572));
#41685=CARTESIAN_POINT('Ctrl Pts',(144.929405430547,-2.05826548570975,339.466847462454));
#41686=CARTESIAN_POINT('Ctrl Pts',(144.92199362637,-1.93981066872105,339.521429908682));
#41687=CARTESIAN_POINT('Ctrl Pts',(144.914581822193,-1.81933292542051,339.571228268232));
#41688=CARTESIAN_POINT('Ctrl Pts',(144.907170018016,-1.69725730241249,339.616113160648));
#41689=CARTESIAN_POINT('Ctrl Pts',(144.899394939238,-1.56919838947214,339.663197995348));
#41690=CARTESIAN_POINT('Ctrl Pts',(144.891619860459,-1.43897631282604,339.705024333909));
#41691=CARTESIAN_POINT('Ctrl Pts',(144.883844781681,-1.30706215420824,339.741389204393));
#41692=CARTESIAN_POINT('Ctrl Pts',(144.876079270632,-1.17531032436078,339.777709325589));
#41693=CARTESIAN_POINT('Ctrl Pts',(144.868313759583,-1.0418709287678,339.808581248059));
#41694=CARTESIAN_POINT('Ctrl Pts',(144.860548248534,-0.907234153928469,
339.833850354784));
#41695=CARTESIAN_POINT('Ctrl Pts',(144.852790437012,-0.77273087184328,339.859094407116));
#41696=CARTESIAN_POINT('Ctrl Pts',(144.845032625489,-0.637032954808813,
339.878746627246));
#41697=CARTESIAN_POINT('Ctrl Pts',(144.837274813967,-0.500644508125581,
339.892702539393));
#41698=CARTESIAN_POINT('Ctrl Pts',(144.829522840444,-0.364358698073604,
339.906647949274));
#41699=CARTESIAN_POINT('Ctrl Pts',(144.821770866921,-0.227383779979994,
339.914905543918));
#41700=CARTESIAN_POINT('Ctrl Pts',(144.814018893398,-0.0902324295267442,
339.917422207942));
#41701=CARTESIAN_POINT('Ctrl Pts',(144.80627020284,0.0468608372481148,339.919937806158));
#41702=CARTESIAN_POINT('Ctrl Pts',(144.798521512283,0.184129997776206,339.916717302258));
#41703=CARTESIAN_POINT('Ctrl Pts',(144.790772821725,0.321059114991753,339.907759581233));
#41704=CARTESIAN_POINT('Ctrl Pts',(144.783025743347,0.457959742960808,339.898803723936));
#41705=CARTESIAN_POINT('Ctrl Pts',(144.77527866497,0.594520078546099,339.884113049318));
#41706=CARTESIAN_POINT('Ctrl Pts',(144.767531586592,0.730226446869954,339.863738520808));
#41707=CARTESIAN_POINT('Ctrl Pts',(144.759784443286,0.865933952543838,339.84336382154));
#41708=CARTESIAN_POINT('Ctrl Pts',(144.75203729998,1.00078709013895,339.817305231398));
#41709=CARTESIAN_POINT('Ctrl Pts',(144.744290156674,1.1342799458554,339.785665269002));
#41710=CARTESIAN_POINT('Ctrl Pts',(144.736541271646,1.26780281359986,339.75401819327));
#41711=CARTESIAN_POINT('Ctrl Pts',(144.728792386618,1.39996441065466,339.716787338477));
#41712=CARTESIAN_POINT('Ctrl Pts',(144.72104350159,1.53027199380604,339.674125660214));
#41713=CARTESIAN_POINT('Ctrl Pts',(144.713286391815,1.66071788677265,339.631418700405));
#41714=CARTESIAN_POINT('Ctrl Pts',(144.70552928204,1.78930546277245,339.583269524141));
#41715=CARTESIAN_POINT('Ctrl Pts',(144.697772172266,1.91555952849149,339.529880214234));
#41716=CARTESIAN_POINT('Ctrl Pts',(144.69001091734,2.04188106034638,339.476462374787));
#41717=CARTESIAN_POINT('Ctrl Pts',(144.682249662413,2.16586624411189,339.417798989215));
#41718=CARTESIAN_POINT('Ctrl Pts',(144.674488407487,2.28706357654228,339.354138635753));
#41719=CARTESIAN_POINT('Ctrl Pts',(144.666714737083,2.40845478520644,339.290376446472));
#41720=CARTESIAN_POINT('Ctrl Pts',(144.658941066678,2.52704889251869,339.221601512071));
#41721=CARTESIAN_POINT('Ctrl Pts',(144.651167396273,2.64242176961468,339.148106827695));
#41722=CARTESIAN_POINT('Ctrl Pts',(144.643755592096,2.7524240115249,339.078033338557));
#41723=CARTESIAN_POINT('Ctrl Pts',(144.636343787919,2.85949793438714,339.003669783716));
#41724=CARTESIAN_POINT('Ctrl Pts',(144.628931983742,2.96330472230804,338.925303578737));
#41725=CARTESIAN_POINT('Ctrl Pts',(144.621156904963,3.07219939012918,338.843096412612));
#41726=CARTESIAN_POINT('Ctrl Pts',(144.613381826185,3.17784268836485,338.756224521984));
#41727=CARTESIAN_POINT('Ctrl Pts',(144.605606747407,3.27980900422639,338.664974209772));
#41728=CARTESIAN_POINT('Ctrl Pts',(144.597841236358,3.38164984404481,338.573836186879));
#41729=CARTESIAN_POINT('Ctrl Pts',(144.590075725309,3.47982241597921,338.478330720999));
#41730=CARTESIAN_POINT('Ctrl Pts',(144.58231021426,3.57393143123928,338.378786348277));
#41731=CARTESIAN_POINT('Ctrl Pts',(144.574552402737,3.66794713713673,338.27934067409));
#41732=CARTESIAN_POINT('Ctrl Pts',(144.566794591215,3.75790703755715,338.175864344624));
#41733=CARTESIAN_POINT('Ctrl Pts',(144.559036779693,3.84345047628596,338.068724734941));
#41734=CARTESIAN_POINT('Ctrl Pts',(144.55128480617,3.92892954086429,337.961665751212));
#41735=CARTESIAN_POINT('Ctrl Pts',(144.543532832647,4.00999851616736,337.850949278638));
#41736=CARTESIAN_POINT('Ctrl Pts',(144.535780859124,4.0863352981092,337.736977693356));
#41737=CARTESIAN_POINT('Ctrl Pts',(144.528032168566,4.1626397513786,337.623054375108));
#41738=CARTESIAN_POINT('Ctrl Pts',(144.520283478009,4.23421578020743,337.505879010058));
#41739=CARTESIAN_POINT('Ctrl Pts',(144.512534787451,4.30078324380866,337.385884857296));
#41740=CARTESIAN_POINT('Ctrl Pts',(144.504787709073,4.36733685749311,337.26591567032));
#41741=CARTESIAN_POINT('Ctrl Pts',(144.497040630695,4.42888378921111,337.143129203753));
#41742=CARTESIAN_POINT('Ctrl Pts',(144.489293552318,4.48518891624504,337.017984996994));
#41743=CARTESIAN_POINT('Ctrl Pts',(144.481546409012,4.54149451517015,336.892839741406));
#41744=CARTESIAN_POINT('Ctrl Pts',(144.473799265706,4.5925580614089,336.76533706267));
#41745=CARTESIAN_POINT('Ctrl Pts',(144.4660521224,4.63819198606711,336.635957873199));
#41746=CARTESIAN_POINT('Ctrl Pts',(144.458303237372,4.68383617020041,336.50654959654));
#41747=CARTESIAN_POINT('Ctrl Pts',(144.450554352344,4.72404817371695,336.375264338199));
#41748=CARTESIAN_POINT('Ctrl Pts',(144.442805467316,4.75868996860927,336.242599229501));
#41749=CARTESIAN_POINT('Ctrl Pts',(144.435048357541,4.79336853266061,336.109793308687));
#41750=CARTESIAN_POINT('Ctrl Pts',(144.427291247766,4.82246497884918,335.975604990658));
#41751=CARTESIAN_POINT('Ctrl Pts',(144.419534137992,4.84589208855476,335.840543234214));
#41752=CARTESIAN_POINT('Ctrl Pts',(144.411772883066,4.86933171695872,335.705409305085));
#41753=CARTESIAN_POINT('Ctrl Pts',(144.404011628139,4.88709592170682,335.569401394912));
#41754=CARTESIAN_POINT('Ctrl Pts',(144.396250373213,4.89914940322585,335.433033702351));
#41755=CARTESIAN_POINT('Ctrl Pts',(144.388476702809,4.91122216638709,335.296447865924));
#41756=CARTESIAN_POINT('Ctrl Pts',(144.380703032404,4.91756593319584,335.159501487682));
#41757=CARTESIAN_POINT('Ctrl Pts',(144.372929361999,4.9181975690542,335.022709783119));
#41758=CARTESIAN_POINT('Ctrl Pts',(144.365517557822,4.9187998021114,334.892285765315));
#41759=CARTESIAN_POINT('Ctrl Pts',(144.358105753645,4.91420974592913,334.762002632754));
#41760=CARTESIAN_POINT('Ctrl Pts',(144.350693949468,4.90448574166947,334.632300840005));
#41761=CARTESIAN_POINT('Ctrl Pts',(144.34291887069,4.89428513499471,334.496241976032));
#41762=CARTESIAN_POINT('Ctrl Pts',(144.335143791911,4.8784023593217,334.360392908018));
#41763=CARTESIAN_POINT('Ctrl Pts',(144.327368713133,4.85684784938132,334.225266477774));
#41764=CARTESIAN_POINT('Ctrl Pts',(144.319603202084,4.83531986363765,334.090306329206));
#41765=CARTESIAN_POINT('Ctrl Pts',(144.311837691035,4.80813409167404,333.956067431356));
#41766=CARTESIAN_POINT('Ctrl Pts',(144.304072179986,4.77535289309746,333.823059980761));
#41767=CARTESIAN_POINT('Ctrl Pts',(144.296314368463,4.7426041971747,333.690184407441));
#41768=CARTESIAN_POINT('Ctrl Pts',(144.288556556941,4.70427120817129,333.558538228622));
#41769=CARTESIAN_POINT('Ctrl Pts',(144.280798745419,4.66046768784341,333.428623535537));
#41770=CARTESIAN_POINT('Ctrl Pts',(144.273046771896,4.61669713105369,333.298806607379));
#41771=CARTESIAN_POINT('Ctrl Pts',(144.265294798373,4.56746436150689,333.170718940296));
#41772=CARTESIAN_POINT('Ctrl Pts',(144.25754282485,4.51293343687854,333.044849147303));
#41773=CARTESIAN_POINT('Ctrl Pts',(144.249794134292,4.45842560612914,332.919032660242));
#41774=CARTESIAN_POINT('Ctrl Pts',(144.242045443735,4.39862423806305,332.795432537042));
#41775=CARTESIAN_POINT('Ctrl Pts',(144.234296753177,4.33374206923738,332.674518815423));
#41776=CARTESIAN_POINT('Ctrl Pts',(144.226549674799,4.26887339968883,332.553630250913));
#41777=CARTESIAN_POINT('Ctrl Pts',(144.218802596422,4.19892621673326,332.43542732044));
#41778=CARTESIAN_POINT('Ctrl Pts',(144.211055518044,4.12415971846065,332.32035642685));
#41779=CARTESIAN_POINT('Ctrl Pts',(144.203308374738,4.04939259357281,332.205284568854));
#41780=CARTESIAN_POINT('Ctrl Pts',(144.195561231432,3.96980628576874,332.093345127863));
#41781=CARTESIAN_POINT('Ctrl Pts',(144.187814088126,3.88570370026562,331.984956083862));
#41782=CARTESIAN_POINT('Ctrl Pts',(144.180065203098,3.80158220671579,331.876542671703));
#41783=CARTESIAN_POINT('Ctrl Pts',(144.17231631807,3.71294265459526,331.771681553625));
#41784=CARTESIAN_POINT('Ctrl Pts',(144.164567433042,3.620128397368,331.670757826611));
#41785=CARTESIAN_POINT('Ctrl Pts',(144.156810323267,3.52721562612911,331.569726978111));
#41786=CARTESIAN_POINT('Ctrl Pts',(144.149053213492,3.4301195633022,331.472642157156));
#41787=CARTESIAN_POINT('Ctrl Pts',(144.141296103718,3.32922100420126,331.379852134555));
#41788=CARTESIAN_POINT('Ctrl Pts',(144.133534848792,3.22826852813645,331.287012527933));
#41789=CARTESIAN_POINT('Ctrl Pts',(144.125773593865,3.12350980536916,331.198472544851));
#41790=CARTESIAN_POINT('Ctrl Pts',(144.118012338939,3.01535813389604,331.11454013187));
#41791=CARTESIAN_POINT('Ctrl Pts',(144.110238668535,2.90703345499511,331.030473454383));
#41792=CARTESIAN_POINT('Ctrl Pts',(144.10246499813,2.79530530013393,330.951029302286));
#41793=CARTESIAN_POINT('Ctrl Pts',(144.094691327725,2.68061605185049,330.876472305772));
#41794=CARTESIAN_POINT('Ctrl Pts',(144.087279523548,2.57126561566729,330.805385955384));
#41795=CARTESIAN_POINT('Ctrl Pts',(144.079867719371,2.45922380725008,330.738742152878));
#41796=CARTESIAN_POINT('Ctrl Pts',(144.072455915194,2.34489258599307,330.676730193169));
#41797=CARTESIAN_POINT('Ctrl Pts',(144.064680836416,2.22495765100707,330.611678842591));
#41798=CARTESIAN_POINT('Ctrl Pts',(144.056905757637,2.10212419023106,330.551519281778));
#41799=CARTESIAN_POINT('Ctrl Pts',(144.049130678859,1.97682911011694,330.496520264074));
#41800=CARTESIAN_POINT('Ctrl Pts',(144.04136516781,1.85168821357553,330.441588926163));
#41801=CARTESIAN_POINT('Ctrl Pts',(144.033599656761,1.72409207938351,330.391805651538));
#41802=CARTESIAN_POINT('Ctrl Pts',(144.025834145712,1.59450348905423,330.347394097294));
#41803=CARTESIAN_POINT('Ctrl Pts',(144.018076334189,1.46504338618959,330.303026577236));
#41804=CARTESIAN_POINT('Ctrl Pts',(144.010318522667,1.33359512597675,330.264020304272));
#41805=CARTESIAN_POINT('Ctrl Pts',(144.002560711145,1.20064249065815,330.230551324091));
#41806=CARTESIAN_POINT('Ctrl Pts',(143.994808737622,1.0677899064138,330.197107530379));
#41807=CARTESIAN_POINT('Ctrl Pts',(143.987056764099,0.93343557795561,330.169192830299));
#41808=CARTESIAN_POINT('Ctrl Pts',(143.979304790576,0.798079171413243,330.146933680789));
#41809=CARTESIAN_POINT('Ctrl Pts',(143.971556100018,0.662780088389454,330.124683958043));
#41810=CARTESIAN_POINT('Ctrl Pts',(143.963807409461,0.526480156235899,330.108085085419));
#41811=CARTESIAN_POINT('Ctrl Pts',(143.956058718903,0.389689763655344,330.097212532589));
#41812=CARTESIAN_POINT('Ctrl Pts',(143.948311640525,0.252927831458461,330.086342241884));
#41813=CARTESIAN_POINT('Ctrl Pts',(143.940564562147,0.115676031208867,330.081195932127));
#41814=CARTESIAN_POINT('Ctrl Pts',(143.93281748377,-0.0215499804572701,
330.08179721231));
#41815=CARTESIAN_POINT('Ctrl Pts',(143.925070340464,-0.158777142209558,
330.082398497532));
#41816=CARTESIAN_POINT('Ctrl Pts',(143.917323197158,-0.295978124076759,
330.088747467059));
#41817=CARTESIAN_POINT('Ctrl Pts',(143.909576053852,-0.432637518377247,
330.100815594388));
#41818=CARTESIAN_POINT('Ctrl Pts',(143.901827168824,-0.569327636610888,
330.112886434888));
#41819=CARTESIAN_POINT('Ctrl Pts',(143.894078283796,-0.705475535705275,
330.130678957386));
#41820=CARTESIAN_POINT('Ctrl Pts',(143.886329398768,-0.840571571131002,
330.154112826705));
#41821=CARTESIAN_POINT('Ctrl Pts',(143.878572288993,-0.975810998884487,
330.177571568974));
#41822=CARTESIAN_POINT('Ctrl Pts',(143.870815179218,-1.10999594700619,330.206683552314));
#41823=CARTESIAN_POINT('Ctrl Pts',(143.863058069444,-1.24262705648704,330.241317297719));
#41824=CARTESIAN_POINT('Ctrl Pts',(143.855296814518,-1.37532903979217,330.27596955029));
#41825=CARTESIAN_POINT('Ctrl Pts',(143.847535559591,-1.50647515642764,330.316149329926));
#41826=CARTESIAN_POINT('Ctrl Pts',(143.839774304665,-1.6355827882982,330.361675733077));
#41827=CARTESIAN_POINT('Ctrl Pts',(143.832000634261,-1.76489695030359,330.407274963637));
#41828=CARTESIAN_POINT('Ctrl Pts',(143.824226963856,-1.89216574822349,330.458237763472));
#41829=CARTESIAN_POINT('Ctrl Pts',(143.816453293451,-2.01692725030957,330.514335330248));
#41830=CARTESIAN_POINT('Ctrl Pts',(143.809041489274,-2.13588107445724,330.567821541795));
#41831=CARTESIAN_POINT('Ctrl Pts',(143.801629685097,-2.25255552125887,330.625975103243));
#41832=CARTESIAN_POINT('Ctrl Pts',(143.79421788092,-2.36657388529132,330.688560436704));
#41833=CARTESIAN_POINT('Ctrl Pts',(143.786442802142,-2.48618062898853,330.754213263789));
#41834=CARTESIAN_POINT('Ctrl Pts',(143.778667723363,-2.60324232093219,330.824950751182));
#41835=CARTESIAN_POINT('Ctrl Pts',(143.770892644585,-2.71729652555157,330.900550932781));
#41836=CARTESIAN_POINT('Ctrl Pts',(143.763127133536,-2.83121037921096,330.976058083543));
#41837=CARTESIAN_POINT('Ctrl Pts',(143.755361622487,-2.94212378659893,331.056415808465));
#41838=CARTESIAN_POINT('Ctrl Pts',(143.747596111438,-3.04959823205991,331.141355978389));
#41839=CARTESIAN_POINT('Ctrl Pts',(143.739838299915,-3.15696611629546,331.226211929886));
#41840=CARTESIAN_POINT('Ctrl Pts',(143.732080488393,-3.26090151949346,331.315641043745));
#41841=CARTESIAN_POINT('Ctrl Pts',(143.724322676871,-3.36099459874852,331.409331765579));
#41842=CARTESIAN_POINT('Ctrl Pts',(143.716570703348,-3.46101235478711,331.502951982173));
#41843=CARTESIAN_POINT('Ctrl Pts',(143.708818729825,-3.55719325799698,331.600827157338));
#41844=CARTESIAN_POINT('Ctrl Pts',(143.701066756302,-3.64916057002648,331.702605544272));
#41845=CARTESIAN_POINT('Ctrl Pts',(143.693318065745,-3.74108893384489,331.804340827999));
#41846=CARTESIAN_POINT('Ctrl Pts',(143.685569375187,-3.82880699413227,331.909975746359));
#41847=CARTESIAN_POINT('Ctrl Pts',(143.677820684629,-3.91197508621941,332.019121943571));
#41848=CARTESIAN_POINT('Ctrl Pts',(143.670073606251,-3.99512587449037,332.128245432006));
#41849=CARTESIAN_POINT('Ctrl Pts',(143.662326527874,-4.07372834077822,332.24087843547));
#41850=CARTESIAN_POINT('Ctrl Pts',(143.654579449496,-4.1474835803845,332.356600103476));
#41851=CARTESIAN_POINT('Ctrl Pts',(143.64683230619,-4.22123943813074,332.472322741342));
#41852=CARTESIAN_POINT('Ctrl Pts',(143.639085162884,-4.29014777808469,332.591133765764));
#41853=CARTESIAN_POINT('Ctrl Pts',(143.631338019578,-4.35395367212233,332.712584322098));
#41854=CARTESIAN_POINT('Ctrl Pts',(143.62358913455,-4.4177739110794,332.834062183095));
#41855=CARTESIAN_POINT('Ctrl Pts',(143.615840249522,-4.47648923968823,332.95818041089));
#41856=CARTESIAN_POINT('Ctrl Pts',(143.608091364494,-4.52989141561629,333.08446696055));
#41857=CARTESIAN_POINT('Ctrl Pts',(143.600334254719,-4.58335027316575,333.210887552058));
#41858=CARTESIAN_POINT('Ctrl Pts',(143.592577144945,-4.63148456025762,333.339480702275));
#41859=CARTESIAN_POINT('Ctrl Pts',(143.58482003517,-4.67413460857986,333.46975533872));
#41860=CARTESIAN_POINT('Ctrl Pts',(143.577058780244,-4.71680744772426,333.600099589766));
#41861=CARTESIAN_POINT('Ctrl Pts',(143.569297525318,-4.75399010270507,333.7321267414));
#41862=CARTESIAN_POINT('Ctrl Pts',(143.561536270392,-4.78557352683102,333.86533305248));
#41863=CARTESIAN_POINT('Ctrl Pts',(143.553762599987,-4.81720747414253,333.998752450246));
#41864=CARTESIAN_POINT('Ctrl Pts',(143.545988929582,-4.84322421775455,334.133354392813));
#41865=CARTESIAN_POINT('Ctrl Pts',(143.538215259178,-4.86356618465578,334.268626613847));
#41866=CARTESIAN_POINT('Ctrl Pts',(143.530803455,-4.88296122810408,334.39760188045));
#41867=CARTESIAN_POINT('Ctrl Pts',(143.523391650823,-4.89719789557304,334.527186140858));
#41868=CARTESIAN_POINT('Ctrl Pts',(143.515979846646,-4.90627043261721,334.656935130732));
#41869=CARTESIAN_POINT('Ctrl Pts',(143.509498647261,-4.91420384803269,334.770393211023));
#41870=CARTESIAN_POINT('Ctrl Pts',(143.503017447875,-4.91820218909899,334.884129643691));
#41871=CARTESIAN_POINT('Ctrl Pts',(143.49653624849,-4.91824957381517,334.997952521813));
#41872=CARTESIAN_POINT('',(146.996536248541,-4.91824999353705,334.999747863625));
#41873=CARTESIAN_POINT('Ctrl Pts',(146.99653624849,-4.9182499935371,334.999747864535));
#41874=CARTESIAN_POINT('Ctrl Pts',(146.988451747308,-4.91825735260103,335.143296556126));
#41875=CARTESIAN_POINT('Ctrl Pts',(146.980367246126,-4.91197577165588,335.286734459456));
#41876=CARTESIAN_POINT('Ctrl Pts',(146.972282744944,-4.8994601760364,335.429503254858));
#41877=CARTESIAN_POINT('Ctrl Pts',(146.96418868747,-4.88692978634548,335.572440810247));
#41878=CARTESIAN_POINT('Ctrl Pts',(146.956094629996,-4.86815071007839,335.714707342739));
#41879=CARTESIAN_POINT('Ctrl Pts',(146.948000572523,-4.84322933887771,335.855752670772));
#41880=CARTESIAN_POINT('Ctrl Pts',(146.939888459662,-4.81825237565734,335.997112628149));
#41881=CARTESIAN_POINT('Ctrl Pts',(146.9317763468,-4.78710578379308,336.137245600314));
#41882=CARTESIAN_POINT('Ctrl Pts',(146.92366423394,-4.74994683805557,336.275612832385));
#41883=CARTESIAN_POINT('Ctrl Pts',(146.915542734325,-4.71274489465739,336.41414017307));
#41884=CARTESIAN_POINT('Ctrl Pts',(146.90742123471,-4.66951681702968,336.550897374038));
#41885=CARTESIAN_POINT('Ctrl Pts',(146.899299735095,-4.62046882424643,336.685363731266));
#41886=CARTESIAN_POINT('Ctrl Pts',(146.891159808995,-4.5713095487968,336.820135172839));
#41887=CARTESIAN_POINT('Ctrl Pts',(146.883019882894,-4.51630408411138,336.952605063933));
#41888=CARTESIAN_POINT('Ctrl Pts',(146.874879956794,-4.45570635164289,337.082273750118));
#41889=CARTESIAN_POINT('Ctrl Pts',(146.86819872384,-4.40596786973402,337.188705514793));
#41890=CARTESIAN_POINT('Ctrl Pts',(146.861517490887,-4.3524627314102,337.293250469534));
#41891=CARTESIAN_POINT('Ctrl Pts',(146.854836257933,-4.2953532843308,337.395646723807));
#41892=CARTESIAN_POINT('Ctrl Pts',(146.847061179155,-4.22889392673633,337.514807206478));
#41893=CARTESIAN_POINT('Ctrl Pts',(146.839286100376,-4.15736721850354,337.631388344973));
#41894=CARTESIAN_POINT('Ctrl Pts',(146.831511021598,-4.08099824474996,337.744929213814));
#41895=CARTESIAN_POINT('Ctrl Pts',(146.823745510549,-4.00472324788034,337.858330363387));
#41896=CARTESIAN_POINT('Ctrl Pts',(146.8159799995,-3.92361805769198,337.968698366077));
#41897=CARTESIAN_POINT('Ctrl Pts',(146.808214488451,-3.83795375971063,338.075596527639));
#41898=CARTESIAN_POINT('Ctrl Pts',(146.800456676929,-3.75237439813021,338.182388699362));
#41899=CARTESIAN_POINT('Ctrl Pts',(146.792698865406,-3.66224516740222,338.285717573409));
#41900=CARTESIAN_POINT('Ctrl Pts',(146.784941053884,-3.56788038358312,338.385175421));
#41901=CARTESIAN_POINT('Ctrl Pts',(146.777189080361,-3.47358661225655,338.484558423406));
#41902=CARTESIAN_POINT('Ctrl Pts',(146.769437106838,-3.37506390012999,338.580075915266));
#41903=CARTESIAN_POINT('Ctrl Pts',(146.761685133315,-3.27266653111475,338.671353543126));
#41904=CARTESIAN_POINT('Ctrl Pts',(146.753936442757,-3.17031252744598,338.762592514856));
#41905=CARTESIAN_POINT('Ctrl Pts',(146.7461877522,-3.06408742173266,338.849594934326));
#41906=CARTESIAN_POINT('Ctrl Pts',(146.738439061642,-2.95438185556877,338.932023768238));
#41907=CARTESIAN_POINT('Ctrl Pts',(146.730691983264,-2.84469911456428,339.014435452142));
#41908=CARTESIAN_POINT('Ctrl Pts',(146.722944904887,-2.73153766577113,339.092275208584));
#41909=CARTESIAN_POINT('Ctrl Pts',(146.715197826509,-2.61532036938624,339.16524698283));
#41910=CARTESIAN_POINT('Ctrl Pts',(146.707450683203,-2.49910209898838,339.23821936865));
#41911=CARTESIAN_POINT('Ctrl Pts',(146.699703539897,-2.37982826094574,339.306323483048));
#41912=CARTESIAN_POINT('Ctrl Pts',(146.691956396591,-2.25794942188029,339.369307436051));
#41913=CARTESIAN_POINT('Ctrl Pts',(146.684207511563,-2.13604318186429,339.432305549184));
#41914=CARTESIAN_POINT('Ctrl Pts',(146.676458626535,-2.01153112260807,339.490181030905));
#41915=CARTESIAN_POINT('Ctrl Pts',(146.668709741507,-1.88488668509718,339.542728832634));
#41916=CARTESIAN_POINT('Ctrl Pts',(146.660952631732,-1.75810782587179,339.595332409143));
#41917=CARTESIAN_POINT('Ctrl Pts',(146.653195521957,-1.62919242878137,339.64259685952));
#41918=CARTESIAN_POINT('Ctrl Pts',(146.645438412183,-1.49863263377112,339.684365836642));
#41919=CARTESIAN_POINT('Ctrl Pts',(146.637677157257,-1.36800307178104,339.726157133769));
#41920=CARTESIAN_POINT('Ctrl Pts',(146.62991590233,-1.23572773770935,339.762447002828));
#41921=CARTESIAN_POINT('Ctrl Pts',(146.622154647404,-1.10231109789111,339.793129802745));
#41922=CARTESIAN_POINT('Ctrl Pts',(146.614380977,-0.968681034929487,339.823861685143));
#41923=CARTESIAN_POINT('Ctrl Pts',(146.606607306595,-0.833906402363296,
339.848968503094));
#41924=CARTESIAN_POINT('Ctrl Pts',(146.59883363619,-0.698499843782523,339.868396145625));
#41925=CARTESIAN_POINT('Ctrl Pts',(146.591421832013,-0.569396493082272,
339.886919426722));
#41926=CARTESIAN_POINT('Ctrl Pts',(146.584010027836,-0.439719010975681,
339.900280335367));
#41927=CARTESIAN_POINT('Ctrl Pts',(146.576598223659,-0.309911690541216,
339.908476118569));
#41928=CARTESIAN_POINT('Ctrl Pts',(146.568823144881,-0.173742126654373,
339.91707360152));
#41929=CARTESIAN_POINT('Ctrl Pts',(146.561048066102,-0.0369993541179618,
339.920014010076));
#41930=CARTESIAN_POINT('Ctrl Pts',(146.553272987324,0.0998072185269236,
339.917237189889));
#41931=CARTESIAN_POINT('Ctrl Pts',(146.545507476275,0.236445441974683,339.914463786757));
#41932=CARTESIAN_POINT('Ctrl Pts',(146.537741965226,0.37314692226037,339.905987161194));
#41933=CARTESIAN_POINT('Ctrl Pts',(146.529976454177,0.509397733943853,339.89179895449));
#41934=CARTESIAN_POINT('Ctrl Pts',(146.522218642655,0.645513452550358,339.877624815435));
#41935=CARTESIAN_POINT('Ctrl Pts',(146.514460831133,0.781179005522254,339.85775040525));
#41936=CARTESIAN_POINT('Ctrl Pts',(146.506703019611,0.915881430575405,339.832219393573));
#41937=CARTESIAN_POINT('Ctrl Pts',(146.498951046088,1.05048248778232,339.806707594793));
#41938=CARTESIAN_POINT('Ctrl Pts',(146.491199072565,1.18412147722747,339.775547739914));
#41939=CARTESIAN_POINT('Ctrl Pts',(146.483447099042,1.31629187375136,339.738835169701));
#41940=CARTESIAN_POINT('Ctrl Pts',(146.475698408484,1.44840629603409,339.702138147283));
#41941=CARTESIAN_POINT('Ctrl Pts',(146.467949717926,1.5790529865786,339.659893191049));
#41942=CARTESIAN_POINT('Ctrl Pts',(146.460201027369,1.7077371283126,339.612246411791));
#41943=CARTESIAN_POINT('Ctrl Pts',(146.452453948991,1.83639449623608,339.564609545844));
#41944=CARTESIAN_POINT('Ctrl Pts',(146.444706870613,1.96308976121095,339.511573228015));
#41945=CARTESIAN_POINT('Ctrl Pts',(146.436959792235,2.08734513058017,339.453332838262));
#41946=CARTESIAN_POINT('Ctrl Pts',(146.429212648929,2.21160154132905,339.395091960398));
#41947=CARTESIAN_POINT('Ctrl Pts',(146.421465505624,2.33341766176053,339.331647089507));
#41948=CARTESIAN_POINT('Ctrl Pts',(146.413718362318,2.45233784476907,339.263240804554));
#41949=CARTESIAN_POINT('Ctrl Pts',(146.40596947729,2.57128476355967,339.194819140416));
#41950=CARTESIAN_POINT('Ctrl Pts',(146.398220592262,2.68733411062261,339.121434037493));
#41951=CARTESIAN_POINT('Ctrl Pts',(146.390471707234,2.80005725014844,339.043372658857));
#41952=CARTESIAN_POINT('Ctrl Pts',(146.382714597459,2.91290003517898,338.965228425067));
#41953=CARTESIAN_POINT('Ctrl Pts',(146.374957487684,3.02240923837369,338.882398223497));
#41954=CARTESIAN_POINT('Ctrl Pts',(146.367200377909,3.128187058937,338.795211296726));
#41955=CARTESIAN_POINT('Ctrl Pts',(146.359439122983,3.23402140378546,338.707977780049));
#41956=CARTESIAN_POINT('Ctrl Pts',(146.351677868057,3.33612010211076,338.616383160118));
#41957=CARTESIAN_POINT('Ctrl Pts',(146.343916613131,3.43412132240092,338.520794484989));
#41958=CARTESIAN_POINT('Ctrl Pts',(146.336142942726,3.53227931270499,338.425052899133));
#41959=CARTESIAN_POINT('Ctrl Pts',(146.328369272322,3.62632645859891,338.32530477514));
#41960=CARTESIAN_POINT('Ctrl Pts',(146.320595601917,3.71593983614847,338.221951923388));
#41961=CARTESIAN_POINT('Ctrl Pts',(146.31318379774,3.80138168941324,338.123410171751));
#41962=CARTESIAN_POINT('Ctrl Pts',(146.305771993563,3.88279308899692,338.021591964816));
#41963=CARTESIAN_POINT('Ctrl Pts',(146.298360189386,3.95993128737131,337.916869428308));
#41964=CARTESIAN_POINT('Ctrl Pts',(146.290585110607,4.04085025863102,337.807014128333));
#41965=CARTESIAN_POINT('Ctrl Pts',(146.282810031829,4.11732227143436,337.693615437419));
#41966=CARTESIAN_POINT('Ctrl Pts',(146.27503495305,4.18902107051601,337.577069175104));
#41967=CARTESIAN_POINT('Ctrl Pts',(146.267269442001,4.2606316396608,337.460666330386));
#41968=CARTESIAN_POINT('Ctrl Pts',(146.259503930952,4.32748047929625,337.341123950735));
#41969=CARTESIAN_POINT('Ctrl Pts',(146.251738419903,4.38928244585868,337.21886968364));
#41970=CARTESIAN_POINT('Ctrl Pts',(146.243980608381,4.45102313559127,337.096736632007));
#41971=CARTESIAN_POINT('Ctrl Pts',(146.236222796859,4.50772673526551,336.971897390471));
#41972=CARTESIAN_POINT('Ctrl Pts',(146.228464985337,4.55915237428648,336.844806952106));
#41973=CARTESIAN_POINT('Ctrl Pts',(146.220713011814,4.61053931388351,336.717812153326));
#41974=CARTESIAN_POINT('Ctrl Pts',(146.212961038291,4.65665605254184,336.588569890611));
#41975=CARTESIAN_POINT('Ctrl Pts',(146.205209064768,4.69730865451637,336.457557706132));
#41976=CARTESIAN_POINT('Ctrl Pts',(146.19746037421,4.73794404008971,336.326601005392));
#41977=CARTESIAN_POINT('Ctrl Pts',(146.189711683653,4.77311977589454,336.193876246255));
#41978=CARTESIAN_POINT('Ctrl Pts',(146.181962993095,4.80269095570401,336.059878599887));
#41979=CARTESIAN_POINT('Ctrl Pts',(146.174215914717,4.83225598298247,335.925908832849));
#41980=CARTESIAN_POINT('Ctrl Pts',(146.166468836339,4.85621868949043,335.790667086807));
#41981=CARTESIAN_POINT('Ctrl Pts',(146.158721757961,4.87448481337984,335.654660879104));
#41982=CARTESIAN_POINT('Ctrl Pts',(146.150974614656,4.89275109035697,335.518653531538));
#41983=CARTESIAN_POINT('Ctrl Pts',(146.14322747135,4.90532063746016,335.381882096929));
#41984=CARTESIAN_POINT('Ctrl Pts',(146.135480328044,4.91215086772375,335.244861012047));
#41985=CARTESIAN_POINT('Ctrl Pts',(146.127731443016,4.91898263356812,335.107809121916));
#41986=CARTESIAN_POINT('Ctrl Pts',(146.119982557988,4.92007249552335,334.970507860139));
#41987=CARTESIAN_POINT('Ctrl Pts',(146.11223367296,4.91542997571179,334.833473076129));
#41988=CARTESIAN_POINT('Ctrl Pts',(146.104476563185,4.91078252828173,334.696292841983));
#41989=CARTESIAN_POINT('Ctrl Pts',(146.09671945341,4.90039055816213,334.559380041875));
#41990=CARTESIAN_POINT('Ctrl Pts',(146.088962343636,4.88431565962564,334.423247367032));
#41991=CARTESIAN_POINT('Ctrl Pts',(146.081201088709,4.86823217117733,334.28704194724));
#41992=CARTESIAN_POINT('Ctrl Pts',(146.073439833783,4.84645976527734,334.151617869095));
#41993=CARTESIAN_POINT('Ctrl Pts',(146.065678578857,4.81911129267469,334.0174780352));
#41994=CARTESIAN_POINT('Ctrl Pts',(146.057904908452,4.79171907142872,333.883123621286));
#41995=CARTESIAN_POINT('Ctrl Pts',(146.050131238048,4.75873305299711,333.750057936457));
#41996=CARTESIAN_POINT('Ctrl Pts',(146.042357567643,4.7203163756295,333.61876997699));
#41997=CARTESIAN_POINT('Ctrl Pts',(146.034945763466,4.6836880038361,333.493593503623));
#41998=CARTESIAN_POINT('Ctrl Pts',(146.027533959289,4.64212328112795,333.370033246777));
#41999=CARTESIAN_POINT('Ctrl Pts',(146.020122155112,4.59580377135082,333.248494716612));
#42000=CARTESIAN_POINT('Ctrl Pts',(146.012347076334,4.54721400442055,333.120999221037));
#42001=CARTESIAN_POINT('Ctrl Pts',(146.004571997555,4.49323802006642,332.995325735542));
#42002=CARTESIAN_POINT('Ctrl Pts',(145.996796918777,4.43403211594032,332.871962815807));
#42003=CARTESIAN_POINT('Ctrl Pts',(145.989031407728,4.37489906844865,332.748751701998));
#42004=CARTESIAN_POINT('Ctrl Pts',(145.981265896679,4.31054907398809,332.627845845622));
#42005=CARTESIAN_POINT('Ctrl Pts',(145.97350038563,4.24118744291114,332.509716454579));
#42006=CARTESIAN_POINT('Ctrl Pts',(145.965742574108,4.17189458409309,332.391704189172));
#42007=CARTESIAN_POINT('Ctrl Pts',(145.957984762585,4.09760017399217,332.276463245618));
#42008=CARTESIAN_POINT('Ctrl Pts',(145.950226951063,4.01855647709236,332.1644424));
#42009=CARTESIAN_POINT('Ctrl Pts',(145.94247497754,3.93957226308123,332.052505853621));
#42010=CARTESIAN_POINT('Ctrl Pts',(145.934723004017,3.85584610056792,331.943784899952));
#42011=CARTESIAN_POINT('Ctrl Pts',(145.926971030494,3.76767461519253,331.838701049168));
#42012=CARTESIAN_POINT('Ctrl Pts',(145.919222339937,3.67954047049339,331.733661701457));
#42013=CARTESIAN_POINT('Ctrl Pts',(145.911473649379,3.58696499800371,331.632256691863));
#42014=CARTESIAN_POINT('Ctrl Pts',(145.903724958821,3.49028618064765,331.534875840654));
#42015=CARTESIAN_POINT('Ctrl Pts',(145.895977880443,3.39362747812715,331.437515250346));
#42016=CARTESIAN_POINT('Ctrl Pts',(145.888230802066,3.29286740409521,331.344177430268));
#42017=CARTESIAN_POINT('Ctrl Pts',(145.880483723688,3.18838173021944,331.255216293976));
#42018=CARTESIAN_POINT('Ctrl Pts',(145.872736580382,3.08389518065287,331.166254412104));
#42019=CARTESIAN_POINT('Ctrl Pts',(145.864989437076,2.97568326657754,331.081669540575));
#42020=CARTESIAN_POINT('Ctrl Pts',(145.85724229377,2.86415554259743,331.001775882931));
#42021=CARTESIAN_POINT('Ctrl Pts',(145.849493408742,2.75260274481735,330.921864263498));
#42022=CARTESIAN_POINT('Ctrl Pts',(145.841744523714,2.63773297143534,330.846646184236));
#42023=CARTESIAN_POINT('Ctrl Pts',(145.833995638686,2.51998516419439,330.776392793507));
#42024=CARTESIAN_POINT('Ctrl Pts',(145.826238528911,2.40211237821431,330.706064835103));
#42025=CARTESIAN_POINT('Ctrl Pts',(145.818481419137,2.28135579237415,330.640712292286));
#42026=CARTESIAN_POINT('Ctrl Pts',(145.810724309362,2.15817987185988,330.58056081576));
#42027=CARTESIAN_POINT('Ctrl Pts',(145.802963054436,2.03493813007217,330.520377196207));
#42028=CARTESIAN_POINT('Ctrl Pts',(145.79520179951,1.90927483548139,330.465400337506));
#42029=CARTESIAN_POINT('Ctrl Pts',(145.787440544583,1.78167395963085,330.415807490509));
#42030=CARTESIAN_POINT('Ctrl Pts',(145.779666874179,1.65386896396384,330.366135311119));
#42031=CARTESIAN_POINT('Ctrl Pts',(145.771893203774,1.52412056344867,330.321864480375));
#42032=CARTESIAN_POINT('Ctrl Pts',(145.764119533369,1.392928248955,330.283122435788));
#42033=CARTESIAN_POINT('Ctrl Pts',(145.756707729192,1.26784296826336,330.246183842697));
#42034=CARTESIAN_POINT('Ctrl Pts',(145.749295925015,1.14144545579727,330.214270959902));
#42035=CARTESIAN_POINT('Ctrl Pts',(145.741884120838,1.0141749683151,330.187450551304));
#42036=CARTESIAN_POINT('Ctrl Pts',(145.73410904206,0.880666575122889,330.159315594587));
#42037=CARTESIAN_POINT('Ctrl Pts',(145.726333963281,0.745775557768737,330.136696017214));
#42038=CARTESIAN_POINT('Ctrl Pts',(145.718558884503,0.609997334773571,330.119724770664));
#42039=CARTESIAN_POINT('Ctrl Pts',(145.710793373454,0.474386195525958,330.102774408314));
#42040=CARTESIAN_POINT('Ctrl Pts',(145.703027862405,0.337890407081227,330.091458595041));
#42041=CARTESIAN_POINT('Ctrl Pts',(145.695262351356,0.201017323427911,330.085859678623));
#42042=CARTESIAN_POINT('Ctrl Pts',(145.687504539833,0.0642799498357178,
330.080266313547));
#42043=CARTESIAN_POINT('Ctrl Pts',(145.679746728311,-0.0728335864743402,
330.080378580922));
#42044=CARTESIAN_POINT('Ctrl Pts',(145.671988916789,-0.209809385332896,
330.08622720465));
#42045=CARTESIAN_POINT('Ctrl Pts',(145.664236943266,-0.346682105559385,
330.092071427103));
#42046=CARTESIAN_POINT('Ctrl Pts',(145.656484969743,-0.483416905702162,
330.103643396942));
#42047=CARTESIAN_POINT('Ctrl Pts',(145.64873299622,-0.619498807707696,330.120921778681));
#42048=CARTESIAN_POINT('Ctrl Pts',(145.640984305662,-0.755523078946614,
330.138192843015));
#42049=CARTESIAN_POINT('Ctrl Pts',(145.633235615105,-0.89089461503863,330.161165463533));
#42050=CARTESIAN_POINT('Ctrl Pts',(145.625486924547,-1.02510270584944,330.189766377299));
#42051=CARTESIAN_POINT('Ctrl Pts',(145.617739846169,-1.15928287354639,330.218361340406));
#42052=CARTESIAN_POINT('Ctrl Pts',(145.609992767792,-1.29229969539579,330.252582186115));
#42053=CARTESIAN_POINT('Ctrl Pts',(145.602245689414,-1.42365220632738,330.292304442945));
#42054=CARTESIAN_POINT('Ctrl Pts',(145.594498546108,-1.55500581811904,330.332027032685));
#42055=CARTESIAN_POINT('Ctrl Pts',(145.586751402802,-1.68469471703088,330.377251012368));
#42056=CARTESIAN_POINT('Ctrl Pts',(145.579004259496,-1.81223304910432,330.427802012354));
#42057=CARTESIAN_POINT('Ctrl Pts',(145.571255374468,-1.93980005450287,330.478364377279));
#42058=CARTESIAN_POINT('Ctrl Pts',(145.56350648944,-2.06521516766474,330.534256001654));
#42059=CARTESIAN_POINT('Ctrl Pts',(145.555757604412,-2.18801283758504,330.59525450394));
#42060=CARTESIAN_POINT('Ctrl Pts',(145.548000494637,-2.31094084622089,330.656317750666));
#42061=CARTESIAN_POINT('Ctrl Pts',(145.540243384862,-2.43124551132059,330.722498529082));
#42062=CARTESIAN_POINT('Ctrl Pts',(145.532486275088,-2.54848572963048,330.793528373046));
#42063=CARTESIAN_POINT('Ctrl Pts',(145.524725020162,-2.66578859736462,330.864596173088));
#42064=CARTESIAN_POINT('Ctrl Pts',(145.516963765235,-2.78002342998789,330.940517985603));
#42065=CARTESIAN_POINT('Ctrl Pts',(145.509202510309,-2.89077926870459,331.020982749205));
#42066=CARTESIAN_POINT('Ctrl Pts',(145.501428839905,-3.00171228066773,331.101576230204));
#42067=CARTESIAN_POINT('Ctrl Pts',(145.4936551695,-3.10915487119704,331.186726941483));
#42068=CARTESIAN_POINT('Ctrl Pts',(145.485881499095,-3.21272957220138,331.276083814262));
#42069=CARTESIAN_POINT('Ctrl Pts',(145.478469694918,-3.31148284595504,331.361281103115));
#42070=CARTESIAN_POINT('Ctrl Pts',(145.471057890741,-3.40672001661188,331.450301575878));
#42071=CARTESIAN_POINT('Ctrl Pts',(145.463646086564,-3.49814723394469,331.54281198195));
#42072=CARTESIAN_POINT('Ctrl Pts',(145.455976271731,-3.59275710367367,331.63854274706));
#42073=CARTESIAN_POINT('Ctrl Pts',(145.448306456898,-3.68360372780343,331.73833168146));
#42074=CARTESIAN_POINT('Ctrl Pts',(145.440636642065,-3.77031161777008,331.841846525672));
#42075=CARTESIAN_POINT('Ctrl Pts',(145.432976460366,-3.8569106043599,331.945231357309));
#42076=CARTESIAN_POINT('Ctrl Pts',(145.425316278667,-3.93938093917433,332.052332486302));
#42077=CARTESIAN_POINT('Ctrl Pts',(145.417656096968,-4.0173827889169,332.162779777702));
#42078=CARTESIAN_POINT('Ctrl Pts',(145.410004775819,-4.09529441373516,332.273099314459));
#42079=CARTESIAN_POINT('Ctrl Pts',(145.40235345467,-4.16874761186798,332.386756982264));
#42080=CARTESIAN_POINT('Ctrl Pts',(145.394702133522,-4.2374422648968,332.503349020354));
#42081=CARTESIAN_POINT('Ctrl Pts',(145.387055773642,-4.306092374942,332.619865457841));
#42082=CARTESIAN_POINT('Ctrl Pts',(145.379409413763,-4.36998987136978,332.739312137212));
#42083=CARTESIAN_POINT('Ctrl Pts',(145.371763053884,-4.42887756327229,332.861255837637));
#42084=CARTESIAN_POINT('Ctrl Pts',(145.364119890709,-4.48774063606745,332.983148557203));
#42085=CARTESIAN_POINT('Ctrl Pts',(145.356476727534,-4.54159789544213,333.107535859778));
#42086=CARTESIAN_POINT('Ctrl Pts',(145.348833564359,-4.59023805793477,333.233959900232));
#42087=CARTESIAN_POINT('Ctrl Pts',(145.341191836263,-4.63886908776217,333.36036020334));
#42088=CARTESIAN_POINT('Ctrl Pts',(145.333550108167,-4.68228482634771,333.488796107685));
#42089=CARTESIAN_POINT('Ctrl Pts',(145.32590838007,-4.72032231776672,333.618790284246));
#42090=CARTESIAN_POINT('Ctrl Pts',(145.318263816003,-4.75837392552262,333.748832703777));
#42091=CARTESIAN_POINT('Ctrl Pts',(145.310619251937,-4.7910431831734,333.880434165006));
#42092=CARTESIAN_POINT('Ctrl Pts',(145.30297468787,-4.8182171885484,334.013102747761));
#42093=CARTESIAN_POINT('Ctrl Pts',(145.295328537929,-4.84539683120244,334.145798852768));
#42094=CARTESIAN_POINT('Ctrl Pts',(145.287682387988,-4.86707888188329,334.279562123726));
#42095=CARTESIAN_POINT('Ctrl Pts',(145.280036238048,-4.88320188790053,334.413892173312));
#42096=CARTESIAN_POINT('Ctrl Pts',(145.272383494346,-4.89933879781132,334.548338064244));
#42097=CARTESIAN_POINT('Ctrl Pts',(145.264730750644,-4.90990705633585,334.683351308939));
#42098=CARTESIAN_POINT('Ctrl Pts',(145.257078006942,-4.91489722135088,334.818428069192));
#42099=CARTESIAN_POINT('Ctrl Pts',(145.253564087473,-4.91718856138322,334.880451426591));
#42100=CARTESIAN_POINT('Ctrl Pts',(145.250050168003,-4.91830455064958,334.942488182909));
#42101=CARTESIAN_POINT('Ctrl Pts',(145.246536248534,-4.91824795069328,335.004489766291));
#42102=CARTESIAN_POINT('',(148.746536238457,-4.91925759883339,334.995611705565));
#42103=CARTESIAN_POINT('Ctrl Pts',(148.746536220508,-4.91824804336388,334.995612922681));
#42104=CARTESIAN_POINT('Ctrl Pts',(148.73888721855,-4.91836834981328,335.130485621825));
#42105=CARTESIAN_POINT('Ctrl Pts',(148.731238216592,-4.91293658427382,335.265537890568));
#42106=CARTESIAN_POINT('Ctrl Pts',(148.723589214634,-4.90193520133637,335.400267840826));
#42107=CARTESIAN_POINT('Ctrl Pts',(148.715946577363,-4.89094297258105,335.534885683133));
#42108=CARTESIAN_POINT('Ctrl Pts',(148.708303940092,-4.87439037787505,335.669181340703));
#42109=CARTESIAN_POINT('Ctrl Pts',(148.700661302821,-4.85231193471425,335.802653069968));
#42110=CARTESIAN_POINT('Ctrl Pts',(148.693022560317,-4.83024474295622,335.936056780662));
#42111=CARTESIAN_POINT('Ctrl Pts',(148.685383817813,-4.80265736764482,336.068637001217));
#42112=CARTESIAN_POINT('Ctrl Pts',(148.677745075309,-4.76963611017469,336.199897678562));
#42113=CARTESIAN_POINT('Ctrl Pts',(148.670108245621,-4.73662312154852,336.331125486957));
#42114=CARTESIAN_POINT('Ctrl Pts',(148.662471415932,-4.69817905405275,336.461034018351));
#42115=CARTESIAN_POINT('Ctrl Pts',(148.654834586243,-4.65444109706652,336.589138488754));
#42116=CARTESIAN_POINT('Ctrl Pts',(148.647197904936,-4.61070398989816,336.717240470118));
#42117=CARTESIAN_POINT('Ctrl Pts',(148.639561223629,-4.56167332821842,336.843538078707));
#42118=CARTESIAN_POINT('Ctrl Pts',(148.631924542323,-4.50753566578765,336.967563285933));
#42119=CARTESIAN_POINT('Ctrl Pts',(148.624286245292,-4.4533865492329,337.091614733674));
#42120=CARTESIAN_POINT('Ctrl Pts',(148.616647948262,-4.39412844508063,337.213392454829));
#42121=CARTESIAN_POINT('Ctrl Pts',(148.609009651231,-4.32999514183211,337.332450456968));
#42122=CARTESIAN_POINT('Ctrl Pts',(148.601363531302,-4.2657961553142,337.451630394489));
#42123=CARTESIAN_POINT('Ctrl Pts',(148.593717411373,-4.19671219166365,337.568084696027));
#42124=CARTESIAN_POINT('Ctrl Pts',(148.586071291445,-4.12302206393855,337.681393690374));
#42125=CARTESIAN_POINT('Ctrl Pts',(148.57842097385,-4.04929148085525,337.794764890556));
#42126=CARTESIAN_POINT('Ctrl Pts',(148.570770656255,-3.97094993260759,337.904987017903));
#42127=CARTESIAN_POINT('Ctrl Pts',(148.563120338661,-3.88831747903655,338.011672333558));
#42128=CARTESIAN_POINT('Ctrl Pts',(148.555458493911,-3.8055605185951,338.118518397856));
#42129=CARTESIAN_POINT('Ctrl Pts',(148.547796649162,-3.71850000186133,338.221816701511));
#42130=CARTESIAN_POINT('Ctrl Pts',(148.540134804412,-3.62749423183861,338.32121493741));
#42131=CARTESIAN_POINT('Ctrl Pts',(148.5348446908,-3.56465938220769,338.389844357334));
#42132=CARTESIAN_POINT('Ctrl Pts',(148.529554577189,-3.49994452278994,338.45661531508));
#42133=CARTESIAN_POINT('Ctrl Pts',(148.524264463577,-3.43347664954062,338.521423172463));
#42134=CARTESIAN_POINT('Ctrl Pts',(148.516489384798,-3.33578631835186,338.616673715949));
#42135=CARTESIAN_POINT('Ctrl Pts',(148.50871430602,-3.23397499366961,338.708006546902));
#42136=CARTESIAN_POINT('Ctrl Pts',(148.500939227242,-3.1283898944596,338.795044101291));
#42137=CARTESIAN_POINT('Ctrl Pts',(148.493173716193,-3.02293472443598,338.881974550428));
#42138=CARTESIAN_POINT('Ctrl Pts',(148.485408205144,-2.91371531857904,338.964619993602));
#42139=CARTESIAN_POINT('Ctrl Pts',(148.477642694094,-2.80111607251189,339.042639213536));
#42140=CARTESIAN_POINT('Ctrl Pts',(148.469884882572,-2.68862846892532,339.120581077185));
#42141=CARTESIAN_POINT('Ctrl Pts',(148.46212707105,-2.57276801326575,339.193905624628));
#42142=CARTESIAN_POINT('Ctrl Pts',(148.454369259528,-2.45395227251279,339.262311732702));
#42143=CARTESIAN_POINT('Ctrl Pts',(148.446617286005,-2.33522594437226,339.33066636301));
#42144=CARTESIAN_POINT('Ctrl Pts',(148.438865312482,-2.21354909517373,339.394109726928));
#42145=CARTESIAN_POINT('Ctrl Pts',(148.431113338959,-2.08936807816185,339.4523840913));
#42146=CARTESIAN_POINT('Ctrl Pts',(148.423364648401,-1.96523965188457,339.510633776443));
#42147=CARTESIAN_POINT('Ctrl Pts',(148.415615957844,-1.83860952020017,339.56371865025));
#42148=CARTESIAN_POINT('Ctrl Pts',(148.407867267286,-1.70994823712798,339.611427120626));
#42149=CARTESIAN_POINT('Ctrl Pts',(148.400120188908,-1.58131372311037,339.659125664856));
#42150=CARTESIAN_POINT('Ctrl Pts',(148.39237311053,-1.45064926454198,339.70144989483));
#42151=CARTESIAN_POINT('Ctrl Pts',(148.384626032152,-1.31844460550187,339.738236685173));
#42152=CARTESIAN_POINT('Ctrl Pts',(148.376878888847,-1.18623883845948,339.775023783825));
#42153=CARTESIAN_POINT('Ctrl Pts',(148.369131745541,-1.05249322176654,339.806273245497));
#42154=CARTESIAN_POINT('Ctrl Pts',(148.361384602235,-0.917711455959071,
339.831872178163));
#42155=CARTESIAN_POINT('Ctrl Pts',(148.353635717207,-0.782899388349155,
339.857476866011));
#42156=CARTESIAN_POINT('Ctrl Pts',(148.345886832179,-0.647051092018016,
339.877428424061));
#42157=CARTESIAN_POINT('Ctrl Pts',(148.338137947151,-0.510678829123992,
339.891665380623));
#42158=CARTESIAN_POINT('Ctrl Pts',(148.330380837376,-0.374161819301003,
339.905917448438));
#42159=CARTESIAN_POINT('Ctrl Pts',(148.322623727601,-0.237120121341795,
339.914442757636));
#42160=CARTESIAN_POINT('Ctrl Pts',(148.314866617827,-0.100070026504685,
339.91723184854));
#42161=CARTESIAN_POINT('Ctrl Pts',(148.3071053629,0.0370533035209075,339.920022429845));
#42162=CARTESIAN_POINT('Ctrl Pts',(148.299344107974,0.174184648779658,339.917070693474));
#42163=CARTESIAN_POINT('Ctrl Pts',(148.291582853048,0.310810368535273,339.908419295182));
#42164=CARTESIAN_POINT('Ctrl Pts',(148.283809182643,0.447654644916372,339.899754057471));
#42165=CARTESIAN_POINT('Ctrl Pts',(148.276035512239,0.583991290578826,339.885370979202));
#42166=CARTESIAN_POINT('Ctrl Pts',(148.268261841834,0.719313527112632,339.865364437759));
#42167=CARTESIAN_POINT('Ctrl Pts',(148.260850037657,0.848336480977584,339.846289205634));
#42168=CARTESIAN_POINT('Ctrl Pts',(148.25343823348,0.976437059057399,339.822102326113));
#42169=CARTESIAN_POINT('Ctrl Pts',(148.246026429303,1.10318864407574,339.79292790245));
#42170=CARTESIAN_POINT('Ctrl Pts',(148.238251350525,1.23615270185096,339.762323553377));
#42171=CARTESIAN_POINT('Ctrl Pts',(148.230476271746,1.36805237761787,339.726133673908));
#42172=CARTESIAN_POINT('Ctrl Pts',(148.222701192968,1.49838226962256,339.684445926316));
#42173=CARTESIAN_POINT('Ctrl Pts',(148.214935681919,1.62855178239806,339.642809478152));
#42174=CARTESIAN_POINT('Ctrl Pts',(148.20717017087,1.75715498624406,339.595688741169));
#42175=CARTESIAN_POINT('Ctrl Pts',(148.199404659821,1.88369692574338,339.5432223096));
#42176=CARTESIAN_POINT('Ctrl Pts',(148.191646848298,2.01011339854131,339.49080789865));
#42177=CARTESIAN_POINT('Ctrl Pts',(148.183889036776,2.1344723154265,339.433058489694));
#42178=CARTESIAN_POINT('Ctrl Pts',(148.176131225254,2.25629448605361,339.370162268693));
#42179=CARTESIAN_POINT('Ctrl Pts',(148.168379251731,2.37802498163404,339.307313379092));
#42180=CARTESIAN_POINT('Ctrl Pts',(148.160627278208,2.49722218477479,339.239325565334));
#42181=CARTESIAN_POINT('Ctrl Pts',(148.152875304685,2.6134278148142,339.166434701187));
#42182=CARTESIAN_POINT('Ctrl Pts',(148.145126614127,2.72958423170021,339.093574706364));
#42183=CARTESIAN_POINT('Ctrl Pts',(148.13737792357,2.84275126489012,339.015815998321));
#42184=CARTESIAN_POINT('Ctrl Pts',(148.129629233012,2.95249633829824,338.93343977135));
#42185=CARTESIAN_POINT('Ctrl Pts',(148.121882154634,3.06221857832727,338.85108068344));
#42186=CARTESIAN_POINT('Ctrl Pts',(148.114135076256,3.16851996231689,338.764106222029));
#42187=CARTESIAN_POINT('Ctrl Pts',(148.106387997879,3.27099828603664,338.672839946859));
#42188=CARTESIAN_POINT('Ctrl Pts',(148.098640854573,3.37347746862351,338.581572906791));
#42189=CARTESIAN_POINT('Ctrl Pts',(148.090893711267,3.47213323513621,338.48601424118));
#42190=CARTESIAN_POINT('Ctrl Pts',(148.083146567961,3.56659807099842,338.386526430201));
#42191=CARTESIAN_POINT('Ctrl Pts',(148.075397682933,3.66108414456091,338.28701625225));
#42192=CARTESIAN_POINT('Ctrl Pts',(148.067648797905,3.75137714349083,338.18357545455));
#42193=CARTESIAN_POINT('Ctrl Pts',(148.059899912877,3.83714816048657,338.07660154342));
#42194=CARTESIAN_POINT('Ctrl Pts',(148.052142803102,3.92301021572605,337.969514089075));
#42195=CARTESIAN_POINT('Ctrl Pts',(148.044385693327,4.00434045632674,337.858886335594));
#42196=CARTESIAN_POINT('Ctrl Pts',(148.036628583553,4.08085153261982,337.745147324137));
#42197=CARTESIAN_POINT('Ctrl Pts',(148.028867328626,4.15740349398574,337.631347534188));
#42198=CARTESIAN_POINT('Ctrl Pts',(148.0211060737,4.22913095541315,337.51443350647));
#42199=CARTESIAN_POINT('Ctrl Pts',(148.013344818774,4.29579182656153,337.394860255912));
#42200=CARTESIAN_POINT('Ctrl Pts',(148.005571148369,4.36255933337902,337.275095727122));
#42201=CARTESIAN_POINT('Ctrl Pts',(147.997797477965,4.42424387797575,337.152663824218));
#42202=CARTESIAN_POINT('Ctrl Pts',(147.99002380756,4.48065057743245,337.028041780993));
#42203=CARTESIAN_POINT('Ctrl Pts',(147.982612003383,4.53443153145845,336.909220923864));
#42204=CARTESIAN_POINT('Ctrl Pts',(147.975200199206,4.58341484167304,336.788409506498));
#42205=CARTESIAN_POINT('Ctrl Pts',(147.967788395029,4.62747400206407,336.666033439857));
#42206=CARTESIAN_POINT('Ctrl Pts',(147.96001331625,4.67369263315157,336.537659357649));
#42207=CARTESIAN_POINT('Ctrl Pts',(147.952238237472,4.71463827438773,336.407157685985));
#42208=CARTESIAN_POINT('Ctrl Pts',(147.944463158694,4.75011114096031,336.275000867068));
#42209=CARTESIAN_POINT('Ctrl Pts',(147.936697647645,4.78554035591227,336.14300667553));
#42210=CARTESIAN_POINT('Ctrl Pts',(147.928932136596,4.81551009575784,336.009361763219));
#42211=CARTESIAN_POINT('Ctrl Pts',(147.921166625547,4.8398690585666,335.874557349995));
#42212=CARTESIAN_POINT('Ctrl Pts',(147.913408814024,4.86420386939277,335.739886595739));
#42213=CARTESIAN_POINT('Ctrl Pts',(147.905651002502,4.88293890501215,335.604059010603));
#42214=CARTESIAN_POINT('Ctrl Pts',(147.89789319098,4.89597309762072,335.467579394193));
#42215=CARTESIAN_POINT('Ctrl Pts',(147.890141217457,4.90899748158607,335.331202483022));
#42216=CARTESIAN_POINT('Ctrl Pts',(147.882389243934,4.91632952469463,335.194174904776));
#42217=CARTESIAN_POINT('Ctrl Pts',(147.874637270411,4.91791957626672,335.057009682271));
#42218=CARTESIAN_POINT('Ctrl Pts',(147.866888579853,4.91950895445101,334.919902549318));
#42219=CARTESIAN_POINT('Ctrl Pts',(147.859139889296,4.91536117313067,334.782658278081));
#42220=CARTESIAN_POINT('Ctrl Pts',(147.851391198738,4.90547860284268,334.645792801382));
#42221=CARTESIAN_POINT('Ctrl Pts',(147.84364412036,4.89559808870599,334.50895580069));
#42222=CARTESIAN_POINT('Ctrl Pts',(147.835897041982,4.87998518703533,334.372497827389));
#42223=CARTESIAN_POINT('Ctrl Pts',(147.828149963605,4.85869433033462,334.236932200342));
#42224=CARTESIAN_POINT('Ctrl Pts',(147.820402820299,4.83740329519608,334.101365437126));
#42225=CARTESIAN_POINT('Ctrl Pts',(147.812655676993,4.81043427075645,333.96669142122));
#42226=CARTESIAN_POINT('Ctrl Pts',(147.804908533687,4.77789319110129,333.833415362296));
#42227=CARTESIAN_POINT('Ctrl Pts',(147.797159648659,4.74534479552042,333.700109340083));
#42228=CARTESIAN_POINT('Ctrl Pts',(147.789410763631,4.70722194465379,333.568202279898));
#42229=CARTESIAN_POINT('Ctrl Pts',(147.781661878603,4.66368091943255,333.438185880388));
#42230=CARTESIAN_POINT('Ctrl Pts',(147.773904768828,4.62009367931724,333.308031480127));
#42231=CARTESIAN_POINT('Ctrl Pts',(147.766147659054,4.57107690119268,333.179772120473));
#42232=CARTESIAN_POINT('Ctrl Pts',(147.758390549279,4.51683587352932,333.053881618683));
#42233=CARTESIAN_POINT('Ctrl Pts',(147.750629294353,4.46256586119521,332.927923845035));
#42234=CARTESIAN_POINT('Ctrl Pts',(147.742868039426,4.403066206135,332.804337803558));
#42235=CARTESIAN_POINT('Ctrl Pts',(147.7351067845,4.3385885311362,332.683573307874));
#42236=CARTESIAN_POINT('Ctrl Pts',(147.727333114096,4.27400771287057,332.562615628354));
#42237=CARTESIAN_POINT('Ctrl Pts',(147.719559443691,4.20443316028766,332.444488851017));
#42238=CARTESIAN_POINT('Ctrl Pts',(147.711785773286,4.13016072713749,332.32961511566));
#42239=CARTESIAN_POINT('Ctrl Pts',(147.704373969109,4.05934569361944,332.220088780321));
#42240=CARTESIAN_POINT('Ctrl Pts',(147.696962164932,3.98426047517631,332.113519679653));
#42241=CARTESIAN_POINT('Ctrl Pts',(147.689550360755,3.90519476976026,332.010244680122));
#42242=CARTESIAN_POINT('Ctrl Pts',(147.681775281977,3.82225381859714,331.901907865224));
#42243=CARTESIAN_POINT('Ctrl Pts',(147.674000203198,3.73467021469701,331.79685385925));
#42244=CARTESIAN_POINT('Ctrl Pts',(147.66622512442,3.64273312976269,331.695506331096));
#42245=CARTESIAN_POINT('Ctrl Pts',(147.658459613371,3.55090917926433,331.594283517527));
#42246=CARTESIAN_POINT('Ctrl Pts',(147.650694102322,3.4547426672061,331.496758393319));
#42247=CARTESIAN_POINT('Ctrl Pts',(147.642928591273,3.35456479269266,331.403324018746));
#42248=CARTESIAN_POINT('Ctrl Pts',(147.635170779751,3.25448624483407,331.309982284629));
#42249=CARTESIAN_POINT('Ctrl Pts',(147.627412968229,3.15040453352937,331.22072349338));
#42250=CARTESIAN_POINT('Ctrl Pts',(147.619655156706,3.04268946194786,331.135905811105));
#42251=CARTESIAN_POINT('Ctrl Pts',(147.611903183183,2.93505544937278,331.051151956825));
#42252=CARTESIAN_POINT('Ctrl Pts',(147.60415120966,2.82379382470928,330.970832800123));
#42253=CARTESIAN_POINT('Ctrl Pts',(147.596399236137,2.70930913095551,330.895267719397));
#42254=CARTESIAN_POINT('Ctrl Pts',(147.58865054558,2.59487292153776,330.819734640528));
#42255=CARTESIAN_POINT('Ctrl Pts',(147.580901855022,2.47721668340389,330.748951848088));
#42256=CARTESIAN_POINT('Ctrl Pts',(147.573153164465,2.35677555830677,330.683196549498));
#42257=CARTESIAN_POINT('Ctrl Pts',(147.565406086087,2.23635949199171,330.617454931846));
#42258=CARTESIAN_POINT('Ctrl Pts',(147.557659007709,2.11316003407813,330.556738914638));
#42259=CARTESIAN_POINT('Ctrl Pts',(147.549911929331,1.98763830189889,330.501280510709));
#42260=CARTESIAN_POINT('Ctrl Pts',(147.542164786025,1.86211551772689,330.445821641986));
#42261=CARTESIAN_POINT('Ctrl Pts',(147.53441764272,1.73427077800145,330.395620632396));
#42262=CARTESIAN_POINT('Ctrl Pts',(147.526670499414,1.60458625132328,330.350861797648));
#42263=CARTESIAN_POINT('Ctrl Pts',(147.518921614386,1.47487256881032,330.306092900165));
#42264=CARTESIAN_POINT('Ctrl Pts',(147.511172729358,1.34331864569536,330.266768739683));
#42265=CARTESIAN_POINT('Ctrl Pts',(147.50342384433,1.21042253443848,330.233023982584));
#42266=CARTESIAN_POINT('Ctrl Pts',(147.495666734555,1.07738536587563,330.199243408451));
#42267=CARTESIAN_POINT('Ctrl Pts',(147.48790962478,0.943003542824317,330.171054163873));
#42268=CARTESIAN_POINT('Ctrl Pts',(147.480152515006,0.807786601694979,330.148540027103));
#42269=CARTESIAN_POINT('Ctrl Pts',(147.472391260079,0.672497404955977,330.126013859498));
#42270=CARTESIAN_POINT('Ctrl Pts',(147.464630005153,0.536372588643611,330.109168890399));
#42271=CARTESIAN_POINT('Ctrl Pts',(147.456868750227,0.399926578155264,330.098036944796));
#42272=CARTESIAN_POINT('Ctrl Pts',(147.449095079823,0.263262298517647,330.086887191708));
#42273=CARTESIAN_POINT('Ctrl Pts',(147.441321409418,0.12627618874179,330.081468739953));
#42274=CARTESIAN_POINT('Ctrl Pts',(147.433547739013,-0.0105166613726054,
330.081761243866));
#42275=CARTESIAN_POINT('Ctrl Pts',(147.426135934836,-0.140941771405292,
330.082040131652));
#42276=CARTESIAN_POINT('Ctrl Pts',(147.418724130659,-0.271190921798768,
330.087510238409));
#42277=CARTESIAN_POINT('Ctrl Pts',(147.411312326482,-0.400824062171299,
330.098110248722));
#42278=CARTESIAN_POINT('Ctrl Pts',(147.403537247703,-0.536810908909002,
330.109229797116));
#42279=CARTESIAN_POINT('Ctrl Pts',(147.395762168925,-0.672549577378057,
330.12602996752));
#42280=CARTESIAN_POINT('Ctrl Pts',(147.387987090146,-0.807527307964116,
330.148496860828));
#42281=CARTESIAN_POINT('Ctrl Pts',(147.380221579097,-0.94233893985986,330.170936107195));
#42282=CARTESIAN_POINT('Ctrl Pts',(147.372456068048,-1.07639111512157,330.199028138108));
#42283=CARTESIAN_POINT('Ctrl Pts',(147.364690556999,-1.20917407013934,330.232707148643));
#42284=CARTESIAN_POINT('Ctrl Pts',(147.356932745477,-1.34182537047099,330.266352766341));
#42285=CARTESIAN_POINT('Ctrl Pts',(147.349174933955,-1.47320957848017,330.30557424425));
#42286=CARTESIAN_POINT('Ctrl Pts',(147.341417122433,-1.60282538293446,330.350254431227));
#42287=CARTESIAN_POINT('Ctrl Pts',(147.33366514891,-1.7323436473856,330.394900994947));
#42288=CARTESIAN_POINT('Ctrl Pts',(147.325913175387,-1.86009578908672,330.444997964386));
#42289=CARTESIAN_POINT('Ctrl Pts',(147.318161201864,-1.98559431450014,330.500377984683));
#42290=CARTESIAN_POINT('Ctrl Pts',(147.310412511306,-2.1110396912131,330.555734551509));
#42291=CARTESIAN_POINT('Ctrl Pts',(147.302663820748,-2.23423299302842,330.616369561736));
#42292=CARTESIAN_POINT('Ctrl Pts',(147.294915130191,-2.35470563014128,330.682067108224));
#42293=CARTESIAN_POINT('Ctrl Pts',(147.287168051813,-2.47515320191574,330.747750985788));
#42294=CARTESIAN_POINT('Ctrl Pts',(147.279420973435,-2.5928808919661,330.818495117497));
#42295=CARTESIAN_POINT('Ctrl Pts',(147.271673895057,-2.70744405870082,330.894037295407));
#42296=CARTESIAN_POINT('Ctrl Pts',(147.263926751751,-2.82200818558557,330.969580106434));
#42297=CARTESIAN_POINT('Ctrl Pts',(147.256179608446,-2.93340740993668,331.049920828695));
#42298=CARTESIAN_POINT('Ctrl Pts',(147.24843246514,-3.04122580764633,331.134753740134));
#42299=CARTESIAN_POINT('Ctrl Pts',(147.240683580112,-3.14906844522087,331.219605723813));
#42300=CARTESIAN_POINT('Ctrl Pts',(147.232934695083,-3.25332834707508,331.308951664684));
#42301=CARTESIAN_POINT('Ctrl Pts',(147.225185810055,-3.35362274461133,331.402445615515));
#42302=CARTESIAN_POINT('Ctrl Pts',(147.21742870028,-3.45402359565694,331.496038801791));
#42303=CARTESIAN_POINT('Ctrl Pts',(147.209671590506,-3.55045024809324,331.593788525966));
#42304=CARTESIAN_POINT('Ctrl Pts',(147.201914480731,-3.64255651161291,331.695311645222));
#42305=CARTESIAN_POINT('Ctrl Pts',(147.194153225805,-3.73471199377463,331.796889015186));
#42306=CARTESIAN_POINT('Ctrl Pts',(147.186391970879,-3.82254223660822,331.902243497975));
#42307=CARTESIAN_POINT('Ctrl Pts',(147.178630715953,-3.90574209270071,332.010959724626));
#42308=CARTESIAN_POINT('Ctrl Pts',(147.170857045548,-3.98907504144831,332.11984986181));
#42309=CARTESIAN_POINT('Ctrl Pts',(147.163083375143,-4.06776257738746,332.232112168836));
#42310=CARTESIAN_POINT('Ctrl Pts',(147.155309704739,-4.14154306497522,332.347302485496));
#42311=CARTESIAN_POINT('Ctrl Pts',(147.147897900562,-4.21188905311404,332.457130665201));
#42312=CARTESIAN_POINT('Ctrl Pts',(147.140486096385,-4.27777441261324,332.569620143148));
#42313=CARTESIAN_POINT('Ctrl Pts',(147.133074292208,-4.33901256840172,332.684367690295));
#42314=CARTESIAN_POINT('Ctrl Pts',(147.124864295878,-4.40684558479657,332.811472632412));
#42315=CARTESIAN_POINT('Ctrl Pts',(147.116654299549,-4.46917147454035,332.94171328728));
#42316=CARTESIAN_POINT('Ctrl Pts',(147.108444303219,-4.52570597472449,333.074599134507));
#42317=CARTESIAN_POINT('Ctrl Pts',(147.100248947627,-4.58213965795952,333.207248008811));
#42318=CARTESIAN_POINT('Ctrl Pts',(147.092053592035,-4.63280240618409,333.342532376197));
#42319=CARTESIAN_POINT('Ctrl Pts',(147.083858236443,-4.67745572456991,333.479937169987));
#42320=CARTESIAN_POINT('Ctrl Pts',(147.07568251851,-4.72200204495912,333.617012715286));
#42321=CARTESIAN_POINT('Ctrl Pts',(147.067506800577,-4.76056755098082,333.756198245452));
#42322=CARTESIAN_POINT('Ctrl Pts',(147.059331082644,-4.79296201278595,333.896959562622));
#42323=CARTESIAN_POINT('Ctrl Pts',(147.051167168358,-4.82530970526421,334.037517656411));
#42324=CARTESIAN_POINT('Ctrl Pts',(147.043003254073,-4.85150403160578,334.179646688232));
#42325=CARTESIAN_POINT('Ctrl Pts',(147.034839339788,-4.87140414900122,334.322796426771));
#42326=CARTESIAN_POINT('Ctrl Pts',(147.026691107238,-4.89126604106112,334.465671194733));
#42327=CARTESIAN_POINT('Ctrl Pts',(147.018542874687,-4.90485778798851,334.609562437749));
#42328=CARTESIAN_POINT('Ctrl Pts',(147.010394642137,-4.91208942193594,334.753909420324));
#42329=CARTESIAN_POINT('Ctrl Pts',(147.005775177605,-4.91618924067846,334.835743825784));
#42330=CARTESIAN_POINT('Ctrl Pts',(147.001155713073,-4.91824578857046,334.917724486486));
#42331=CARTESIAN_POINT('Ctrl Pts',(146.996536248541,-4.91824999353705,334.999747863625));
#42332=CARTESIAN_POINT('',(150.496536287082,-4.92151798553658,335.002527853233));
#42333=CARTESIAN_POINT('Ctrl Pts',(150.49653624849,-4.92474948212452,335.002530191525));
#42334=CARTESIAN_POINT('Ctrl Pts',(150.488334400158,-4.92565302976486,335.146822327));
#42335=CARTESIAN_POINT('Ctrl Pts',(150.387386540402,-4.85438643557772,336.921856051074));
#42336=CARTESIAN_POINT('Ctrl Pts',(150.193692669221,-2.70353245624263,340.149306858644));
#42337=CARTESIAN_POINT('Ctrl Pts',(149.915454634947,2.86712545234502,340.060043528167));
#42338=CARTESIAN_POINT('Ctrl Pts',(149.637216600673,5.80666465201795,335.327252938012));
#42339=CARTESIAN_POINT('Ctrl Pts',(149.358978566399,3.41751340676379,330.294147156888));
#42340=CARTESIAN_POINT('Ctrl Pts',(149.080740532125,-2.10783944946231,329.579533071615));
#42341=CARTESIAN_POINT('Ctrl Pts',(148.876593092822,-4.74262473034225,332.704915984254));
#42342=CARTESIAN_POINT('Ctrl Pts',(148.765191664944,-4.92286447585139,334.666557075651));
#42343=CARTESIAN_POINT('Ctrl Pts',(148.74653624849,-4.91982192786215,334.995611025212));
#42344=CARTESIAN_POINT('',(152.246536248436,-4.91824906311658,335.003035729386));
#42345=CARTESIAN_POINT('Ctrl Pts',(152.246536248436,-4.91824906311658,335.003035729386));
#42346=CARTESIAN_POINT('Ctrl Pts',(152.237771470162,-4.91815313595883,335.158449336348));
#42347=CARTESIAN_POINT('Ctrl Pts',(152.229006691887,-4.91068658036438,335.313587684498));
#42348=CARTESIAN_POINT('Ctrl Pts',(152.220241913612,-4.89595254032275,335.467794597454));
#42349=CARTESIAN_POINT('Ctrl Pts',(152.211507220859,-4.8812690755803,335.621472187785));
#42350=CARTESIAN_POINT('Ctrl Pts',(152.202772528106,-4.85936810387403,335.774224550554));
#42351=CARTESIAN_POINT('Ctrl Pts',(152.194037835353,-4.83040182517022,335.925419510218));
#42352=CARTESIAN_POINT('Ctrl Pts',(152.185256280418,-4.80128014053808,336.07742564046));
#42353=CARTESIAN_POINT('Ctrl Pts',(152.176474725482,-4.7650172323429,336.227857418963));
#42354=CARTESIAN_POINT('Ctrl Pts',(152.167693170547,-4.72181658489604,336.376092729833));
#42355=CARTESIAN_POINT('Ctrl Pts',(152.158915083411,-4.678632997204,336.5242695032));
#42356=CARTESIAN_POINT('Ctrl Pts',(152.150136996275,-4.62851729139738,336.67025138024));
#42357=CARTESIAN_POINT('Ctrl Pts',(152.141358909139,-4.57171947922819,336.813439843432));
#42358=CARTESIAN_POINT('Ctrl Pts',(152.13358383036,-4.52141154115342,336.940267199348));
#42359=CARTESIAN_POINT('Ctrl Pts',(152.125808751582,-4.46574249469378,337.06519993769));
#42360=CARTESIAN_POINT('Ctrl Pts',(152.118033672803,-4.4048752241667,337.187751659129));
#42361=CARTESIAN_POINT('Ctrl Pts',(152.110268161754,-4.344082854691,337.310152572873));
#42362=CARTESIAN_POINT('Ctrl Pts',(152.102502650705,-4.27810516104536,337.430177952832));
#42363=CARTESIAN_POINT('Ctrl Pts',(152.094737139656,-4.20715380138612,337.54735940809));
#42364=CARTESIAN_POINT('Ctrl Pts',(152.086979328134,-4.1362727902066,337.664424677593));
#42365=CARTESIAN_POINT('Ctrl Pts',(152.079221516612,-4.06042812793231,337.778651301669));
#42366=CARTESIAN_POINT('Ctrl Pts',(152.07146370509,-3.97987811948626,337.889593953575));
#42367=CARTESIAN_POINT('Ctrl Pts',(152.063711731567,-3.89938872747609,338.000453117616));
#42368=CARTESIAN_POINT('Ctrl Pts',(152.055959758044,-3.8142012660504,338.10803291345));
#42369=CARTESIAN_POINT('Ctrl Pts',(152.048207784521,-3.72461802884623,338.21191587712));
#42370=CARTESIAN_POINT('Ctrl Pts',(152.040459093963,-3.63507273019601,338.315754846293));
#42371=CARTESIAN_POINT('Ctrl Pts',(152.032710403405,-3.54113561311906,338.415899801796));
#42372=CARTESIAN_POINT('Ctrl Pts',(152.024961712848,-3.44314989659545,338.511965525468));
#42373=CARTESIAN_POINT('Ctrl Pts',(152.01721463447,-3.34518456681849,338.608011261864));
#42374=CARTESIAN_POINT('Ctrl Pts',(152.009467556092,-3.24317259201413,338.69997918112));
#42375=CARTESIAN_POINT('Ctrl Pts',(152.001720477714,-3.13749449131678,338.787520479081));
#42376=CARTESIAN_POINT('Ctrl Pts',(151.993973334408,-3.03181550493526,338.875062510722));
#42377=CARTESIAN_POINT('Ctrl Pts',(151.986226191103,-2.92247063238652,338.958177597719));
#42378=CARTESIAN_POINT('Ctrl Pts',(151.978479047797,-2.80987363613107,339.036557098751));
#42379=CARTESIAN_POINT('Ctrl Pts',(151.970730162769,-2.69725132568067,339.114954221158));
#42380=CARTESIAN_POINT('Ctrl Pts',(151.962981277741,-2.58137575736353,339.188613415776));
#42381=CARTESIAN_POINT('Ctrl Pts',(151.955232392713,-2.46268949637323,339.257269489585));
#42382=CARTESIAN_POINT('Ctrl Pts',(151.947475282938,-2.34387726055889,339.325998435661));
#42383=CARTESIAN_POINT('Ctrl Pts',(151.939718173163,-2.22224871153101,339.389713456949));
#42384=CARTESIAN_POINT('Ctrl Pts',(151.931961063388,-2.09827132087224,339.448195198786));
#42385=CARTESIAN_POINT('Ctrl Pts',(151.924199808462,-1.97422768065998,339.506708191396));
#42386=CARTESIAN_POINT('Ctrl Pts',(151.916438553536,-1.84783305783023,339.559982180544));
#42387=CARTESIAN_POINT('Ctrl Pts',(151.90867729861,-1.71957377460646,339.607846470553));
#42388=CARTESIAN_POINT('Ctrl Pts',(151.900903628205,-1.59110931832913,339.655787327826));
#42389=CARTESIAN_POINT('Ctrl Pts',(151.893129957801,-1.46077461284239,339.698301071917));
#42390=CARTESIAN_POINT('Ctrl Pts',(151.885356287396,-1.32907082524571,339.735267025626));
#42391=CARTESIAN_POINT('Ctrl Pts',(151.877944483219,-1.20349788064487,339.770512205297));
#42392=CARTESIAN_POINT('Ctrl Pts',(151.870532679042,-1.07668072700208,339.800714403701));
#42393=CARTESIAN_POINT('Ctrl Pts',(151.863120874864,-0.949059483035493,
339.825812797878));
#42394=CARTESIAN_POINT('Ctrl Pts',(151.855345796086,-0.815183141740809,
339.852141339117));
#42395=CARTESIAN_POINT('Ctrl Pts',(151.847570717307,-0.679998821417218,
339.872936323657));
#42396=CARTESIAN_POINT('Ctrl Pts',(151.839795638529,-0.544003691687033,
339.888071505812));
#42397=CARTESIAN_POINT('Ctrl Pts',(151.83203012748,-0.408175912621808,339.903188063161));
#42398=CARTESIAN_POINT('Ctrl Pts',(151.824264616431,-0.271539694153764,
339.912658633153));
#42399=CARTESIAN_POINT('Ctrl Pts',(151.816499105382,-0.13460345657086,339.916407730445));
#42400=CARTESIAN_POINT('Ctrl Pts',(151.80874129386,0.00219700833375552,
339.920153110496));
#42401=CARTESIAN_POINT('Ctrl Pts',(151.800983482338,0.139296512160548,339.918188296525));
#42402=CARTESIAN_POINT('Ctrl Pts',(151.793225670815,0.276180786534392,339.910489510797));
#42403=CARTESIAN_POINT('Ctrl Pts',(151.785473697292,0.41296205115092,339.90279651865));
#42404=CARTESIAN_POINT('Ctrl Pts',(151.777721723769,0.54952802001571,339.889378165396));
#42405=CARTESIAN_POINT('Ctrl Pts',(151.769969750246,0.685364050348281,339.870262742501));
#42406=CARTESIAN_POINT('Ctrl Pts',(151.762221059689,0.821142554041314,339.851155414999));
#42407=CARTESIAN_POINT('Ctrl Pts',(151.754472369131,0.95619134778373,339.826355870927));
#42408=CARTESIAN_POINT('Ctrl Pts',(151.746723678574,1.09000075792248,339.795944266798));
#42409=CARTESIAN_POINT('Ctrl Pts',(151.738976600196,1.22378232789584,339.765538990056));
#42410=CARTESIAN_POINT('Ctrl Pts',(151.731229521818,1.35632464626067,339.729524062341));
#42411=CARTESIAN_POINT('Ctrl Pts',(151.72348244344,1.48712847542296,339.688030712366));
#42412=CARTESIAN_POINT('Ctrl Pts',(151.715735300134,1.61793340084729,339.646537014637));
#42413=CARTESIAN_POINT('Ctrl Pts',(151.707988156829,1.74699943542992,339.599564921257));
#42414=CARTESIAN_POINT('Ctrl Pts',(151.700241013523,1.87384312548903,339.547295350377));
#42415=CARTESIAN_POINT('Ctrl Pts',(151.692492128495,2.00071533270255,339.495014028187));
#42416=CARTESIAN_POINT('Ctrl Pts',(151.684743243467,2.12536383986188,339.437433007463));
#42417=CARTESIAN_POINT('Ctrl Pts',(151.676994358438,2.24732614308001,339.374780939559));
#42418=CARTESIAN_POINT('Ctrl Pts',(151.669237248664,2.369417898347,339.312062372102));
#42419=CARTESIAN_POINT('Ctrl Pts',(151.661480138889,2.48881740597233,339.244262184379));
#42420=CARTESIAN_POINT('Ctrl Pts',(151.653723029114,2.60508723024303,339.171654777822));
#42421=CARTESIAN_POINT('Ctrl Pts',(151.645961774188,2.72141918539019,339.099008572188));
#42422=CARTESIAN_POINT('Ctrl Pts',(151.638200519262,2.83461780235072,339.021550249728));
#42423=CARTESIAN_POINT('Ctrl Pts',(151.630439264336,2.94427636262732,338.939596395949));
#42424=CARTESIAN_POINT('Ctrl Pts',(151.622665593931,3.05411034086269,338.857511442713));
#42425=CARTESIAN_POINT('Ctrl Pts',(151.614891923527,3.1603926430021,338.770916834665));
#42426=CARTESIAN_POINT('Ctrl Pts',(151.607118253122,3.26275057874034,338.680168708555));
#42427=CARTESIAN_POINT('Ctrl Pts',(151.599706448945,3.36034372794295,338.59364492955));
#42428=CARTESIAN_POINT('Ctrl Pts',(151.592294644768,3.45436943951627,338.503345822087));
#42429=CARTESIAN_POINT('Ctrl Pts',(151.584882840591,3.54453839264294,338.409608576594));
#42430=CARTESIAN_POINT('Ctrl Pts',(151.577107761812,3.63912679476281,338.311276989468));
#42431=CARTESIAN_POINT('Ctrl Pts',(151.569332683034,3.72976973350651,338.208850969828));
#42432=CARTESIAN_POINT('Ctrl Pts',(151.561557604256,3.81609199917105,338.10268027943));
#42433=CARTESIAN_POINT('Ctrl Pts',(151.553792093207,3.90230803979211,337.996640238825));
#42434=CARTESIAN_POINT('Ctrl Pts',(151.546026582158,3.98421374214145,337.886864996553));
#42435=CARTESIAN_POINT('Ctrl Pts',(151.538261071109,4.06147049359346,337.773741244631));
#42436=CARTESIAN_POINT('Ctrl Pts',(151.530503259587,4.13865064475154,337.660729655239));
#42437=CARTESIAN_POINT('Ctrl Pts',(151.522745448064,4.21119079905411,337.544376484));
#42438=CARTESIAN_POINT('Ctrl Pts',(151.514987636542,4.27879266117119,337.425101322668));
#42439=CARTESIAN_POINT('Ctrl Pts',(151.507235663019,4.34634365074317,337.305915919678));
#42440=CARTESIAN_POINT('Ctrl Pts',(151.499483689496,4.40896355312974,337.183813242061));
#42441=CARTESIAN_POINT('Ctrl Pts',(151.491731715973,4.46639765649051,337.059241374049));
#42442=CARTESIAN_POINT('Ctrl Pts',(151.483983025416,4.52380743647445,336.934722262297));
#42443=CARTESIAN_POINT('Ctrl Pts',(151.476234334858,4.57603562218161,336.807736394205));
#42444=CARTESIAN_POINT('Ctrl Pts',(151.4684856443,4.62287380527458,336.678755742509));
#42445=CARTESIAN_POINT('Ctrl Pts',(151.460738565922,4.66970224329234,336.549801926315));
#42446=CARTESIAN_POINT('Ctrl Pts',(151.452991487545,4.71114277597546,336.418854519213));
#42447=CARTESIAN_POINT('Ctrl Pts',(151.445244409167,4.74703559024165,336.286404356133));
#42448=CARTESIAN_POINT('Ctrl Pts',(151.437497265861,4.78292870532418,336.153953082994));
#42449=CARTESIAN_POINT('Ctrl Pts',(151.429750122555,4.81327390701554,336.019999406025));
#42450=CARTESIAN_POINT('Ctrl Pts',(151.422002979249,4.83796170872064,335.885047776932));
#42451=CARTESIAN_POINT('Ctrl Pts',(151.414254094221,4.86265506076768,335.750065807849));
#42452=CARTESIAN_POINT('Ctrl Pts',(151.406505209193,4.88168841155758,335.614085824607));
#42453=CARTESIAN_POINT('Ctrl Pts',(151.398756324165,4.89500375150042,335.477620492961));
#42454=CARTESIAN_POINT('Ctrl Pts',(151.39099921439,4.90833322448267,335.341010315603));
#42455=CARTESIAN_POINT('Ctrl Pts',(151.383242104616,4.9159325248913,335.203914150413));
#42456=CARTESIAN_POINT('Ctrl Pts',(151.375484994841,4.91779568118029,335.066848340776));
#42457=CARTESIAN_POINT('Ctrl Pts',(151.367723739915,4.91965983308043,334.929709287552));
#42458=CARTESIAN_POINT('Ctrl Pts',(151.359962484989,4.9157817441957,334.792601012723));
#42459=CARTESIAN_POINT('Ctrl Pts',(151.352201230063,4.90620753931681,334.656036857133));
#42460=CARTESIAN_POINT('Ctrl Pts',(151.344427559658,4.89661801883033,334.5192542434));
#42461=CARTESIAN_POINT('Ctrl Pts',(151.336653889253,4.88131421767315,334.383017876885));
#42462=CARTESIAN_POINT('Ctrl Pts',(151.328880218849,4.8603939347265,334.247833886848));
#42463=CARTESIAN_POINT('Ctrl Pts',(151.321468414671,4.84044749598381,334.118942744068));
#42464=CARTESIAN_POINT('Ctrl Pts',(151.314056610494,4.81539575779751,333.991008488843));
#42465=CARTESIAN_POINT('Ctrl Pts',(151.306644806317,4.78536570269473,333.864456890306));
#42466=CARTESIAN_POINT('Ctrl Pts',(151.298869727538,4.7538637851369,333.73170262095));
#42467=CARTESIAN_POINT('Ctrl Pts',(151.29109464876,4.71678365530317,333.600050443547));
#42468=CARTESIAN_POINT('Ctrl Pts',(151.283319569982,4.67421638781622,333.470005156097));
#42469=CARTESIAN_POINT('Ctrl Pts',(151.275554058933,4.63170150206187,333.340119897652));
#42470=CARTESIAN_POINT('Ctrl Pts',(151.267788547884,4.5837130341727,333.21183796267));
#42471=CARTESIAN_POINT('Ctrl Pts',(151.260023036835,4.53039291899408,333.085653358969));
#42472=CARTESIAN_POINT('Ctrl Pts',(151.252265225312,4.47712567086492,332.959593867669));
#42473=CARTESIAN_POINT('Ctrl Pts',(151.24450741379,4.41853744673061,332.835627927039));
#42474=CARTESIAN_POINT('Ctrl Pts',(151.236749602268,4.35481966552782,332.714233445158));
#42475=CARTESIAN_POINT('Ctrl Pts',(151.228997628745,4.29114983397599,332.592930316475));
#42476=CARTESIAN_POINT('Ctrl Pts',(151.221245655222,4.22235830973238,332.474195139512));
#42477=CARTESIAN_POINT('Ctrl Pts',(151.213493681699,4.14868405719308,332.35848459098));
#42478=CARTESIAN_POINT('Ctrl Pts',(151.205744991141,4.07504100574346,332.242823045933));
#42479=CARTESIAN_POINT('Ctrl Pts',(151.197996300584,3.99651954827849,332.13018391066));
#42480=CARTESIAN_POINT('Ctrl Pts',(151.190247610026,3.91340379503152,332.020997851707));
#42481=CARTESIAN_POINT('Ctrl Pts',(151.182500531648,3.83030533471121,331.911834509826));
#42482=CARTESIAN_POINT('Ctrl Pts',(151.17475345327,3.74261471653039,331.806123126054));
#42483=CARTESIAN_POINT('Ctrl Pts',(151.167006374892,3.65065821002524,331.704263709567));
#42484=CARTESIAN_POINT('Ctrl Pts',(151.159259231587,3.55870093283603,331.6024034394));
#42485=CARTESIAN_POINT('Ctrl Pts',(151.151512088281,3.46247795793816,331.504395491043));
#42486=CARTESIAN_POINT('Ctrl Pts',(151.143764944975,3.36235424005557,331.410604921873));
#42487=CARTESIAN_POINT('Ctrl Pts',(151.136016059947,3.26220801223553,331.316793266592));
#42488=CARTESIAN_POINT('Ctrl Pts',(151.128267174919,3.15815958156755,331.227201144393));
#42489=CARTESIAN_POINT('Ctrl Pts',(151.120518289891,3.0506086673033,331.142154769632));
#42490=CARTESIAN_POINT('Ctrl Pts',(151.112761180116,2.94294359738744,331.05701812577));
#42491=CARTESIAN_POINT('Ctrl Pts',(151.105004070341,2.83176892475961,330.976437110372));
#42492=CARTESIAN_POINT('Ctrl Pts',(151.097246960566,2.71751562204035,330.900696168071));
#42493=CARTESIAN_POINT('Ctrl Pts',(151.08948570564,2.60320126600928,330.824914752232));
#42494=CARTESIAN_POINT('Ctrl Pts',(151.081724450714,2.48580533620802,330.75397876513));
#42495=CARTESIAN_POINT('Ctrl Pts',(151.073963195788,2.36578447267566,330.68812721763));
#42496=CARTESIAN_POINT('Ctrl Pts',(151.066189525383,2.24557161487636,330.622170329115));
#42497=CARTESIAN_POINT('Ctrl Pts',(151.058415854978,2.12272578286044,330.561314306838));
#42498=CARTESIAN_POINT('Ctrl Pts',(151.050642184574,1.99772551610582,330.505750805218));
#42499=CARTESIAN_POINT('Ctrl Pts',(151.043230380397,1.87854404184419,330.452773797967));
#42500=CARTESIAN_POINT('Ctrl Pts',(151.03581857622,1.75740446427026,330.404607772696));
#42501=CARTESIAN_POINT('Ctrl Pts',(151.028406772043,1.63473353926475,330.361376355199));
#42502=CARTESIAN_POINT('Ctrl Pts',(151.020631693264,1.50605014680464,330.31602603715));
#42503=CARTESIAN_POINT('Ctrl Pts',(151.012856614486,1.37527483624023,330.275962962004));
#42504=CARTESIAN_POINT('Ctrl Pts',(151.005081535708,1.24288138868291,330.241383718331));
#42505=CARTESIAN_POINT('Ctrl Pts',(150.997316024659,1.11065085969133,330.206847026618));
#42506=CARTESIAN_POINT('Ctrl Pts',(150.98955051361,0.976806530237054,330.17778083722));
#42507=CARTESIAN_POINT('Ctrl Pts',(150.98178500256,0.841840631123751,330.154333130075));
#42508=CARTESIAN_POINT('Ctrl Pts',(150.974027191038,0.707008551092452,330.1309086714));
#42509=CARTESIAN_POINT('Ctrl Pts',(150.966269379516,0.571057497048823,330.11309167536));
#42510=CARTESIAN_POINT('Ctrl Pts',(150.958511567994,0.434492939863328,330.100979797173));
#42511=CARTESIAN_POINT('Ctrl Pts',(150.950759594471,0.298031151837965,330.088877033558));
#42512=CARTESIAN_POINT('Ctrl Pts',(150.943007620948,0.160957167401659,330.08247087662));
#42513=CARTESIAN_POINT('Ctrl Pts',(150.935255647425,0.0237843330877862,
330.08180751007));
#42514=CARTESIAN_POINT('Ctrl Pts',(150.927506956867,-0.113330408449408,
330.081144424457));
#42515=CARTESIAN_POINT('Ctrl Pts',(150.91975826631,-0.250543526545395,330.086219293893));
#42516=CARTESIAN_POINT('Ctrl Pts',(150.912009575752,-0.387339116163727,
330.097026262401));
#42517=CARTESIAN_POINT('Ctrl Pts',(150.904262497374,-0.524106244317147,
330.107830982429));
#42518=CARTESIAN_POINT('Ctrl Pts',(150.896515418996,-0.660455627368479,
330.124365398577));
#42519=CARTESIAN_POINT('Ctrl Pts',(150.888768340618,-0.795874325900693,
330.14657161175));
#42520=CARTESIAN_POINT('Ctrl Pts',(150.881021197313,-0.931294159371987,
330.168778011032));
#42521=CARTESIAN_POINT('Ctrl Pts',(150.873274054007,-1.06578290704377,330.1966562389));
#42522=CARTESIAN_POINT('Ctrl Pts',(150.865526910701,-1.19883608643651,330.230096950633));
#42523=CARTESIAN_POINT('Ctrl Pts',(150.857778025673,-1.3319191790086,330.263545180549));
#42524=CARTESIAN_POINT('Ctrl Pts',(150.850029140645,-1.46356568206226,330.302558287556));
#42525=CARTESIAN_POINT('Ctrl Pts',(150.842280255617,-1.59328496396169,330.346976672516));
#42526=CARTESIAN_POINT('Ctrl Pts',(150.834523145842,-1.72314193124734,330.391442203608));
#42527=CARTESIAN_POINT('Ctrl Pts',(150.826766036067,-1.85106722077621,330.441324346459));
#42528=CARTESIAN_POINT('Ctrl Pts',(150.819008926292,-1.97658841297388,330.496414616309));
#42529=CARTESIAN_POINT('Ctrl Pts',(150.811247671366,-2.10217667968327,330.551534324638));
#42530=CARTESIAN_POINT('Ctrl Pts',(150.80348641644,-2.22535793838321,330.611867533612));
#42531=CARTESIAN_POINT('Ctrl Pts',(150.795725161514,-2.34568408561011,330.677159587376));
#42532=CARTESIAN_POINT('Ctrl Pts',(150.787951491109,-2.46620271545834,330.742556087147));
#42533=CARTESIAN_POINT('Ctrl Pts',(150.780177820705,-2.58385677149312,330.812927082518));
#42534=CARTESIAN_POINT('Ctrl Pts',(150.7724041503,-2.69822612225555,330.887973874636));
#42535=CARTESIAN_POINT('Ctrl Pts',(150.764992346123,-2.80727155222481,330.959527220526));
#42536=CARTESIAN_POINT('Ctrl Pts',(150.757580541946,-2.91333096686714,331.035330675669));
#42537=CARTESIAN_POINT('Ctrl Pts',(150.750168737769,-3.01606946452102,331.115092272951));
#42538=CARTESIAN_POINT('Ctrl Pts',(150.742483981885,-3.12259147393376,331.197791220381));
#42539=CARTESIAN_POINT('Ctrl Pts',(150.734799226001,-3.22589699379611,331.285020276609));
#42540=CARTESIAN_POINT('Ctrl Pts',(150.727114470118,-3.3255695308752,331.376497501337));
#42541=CARTESIAN_POINT('Ctrl Pts',(150.719439211367,-3.42511888859246,331.467861674803));
#42542=CARTESIAN_POINT('Ctrl Pts',(150.711763952616,-3.52104390063296,331.563463307134));
#42543=CARTESIAN_POINT('Ctrl Pts',(150.704088693865,-3.61295851277673,331.662978296826));
#42544=CARTESIAN_POINT('Ctrl Pts',(150.696420980401,-3.7047827667819,331.762395456706));
#42545=CARTESIAN_POINT('Ctrl Pts',(150.688753266937,-3.79260419319596,331.865718028775));
#42546=CARTESIAN_POINT('Ctrl Pts',(150.681085553473,-3.87607157639534,331.972583246865));
#42547=CARTESIAN_POINT('Ctrl Pts',(150.673396002333,-3.95977667500354,332.079752817483));
#42548=CARTESIAN_POINT('Ctrl Pts',(150.665706451194,-4.03910259183008,332.190484969602));
#42549=CARTESIAN_POINT('Ctrl Pts',(150.658016900054,-4.11373364393594,332.30437788827));
#42550=CARTESIAN_POINT('Ctrl Pts',(150.650357840518,-4.1880687593316,332.417819183991));
#42551=CARTESIAN_POINT('Ctrl Pts',(150.642698780982,-4.25774595314952,332.534395888207));
#42552=CARTESIAN_POINT('Ctrl Pts',(150.635039721446,-4.32249528753078,332.653679998002));
#42553=CARTESIAN_POINT('Ctrl Pts',(150.627381925982,-4.38723393550335,332.772944420819));
#42554=CARTESIAN_POINT('Ctrl Pts',(150.619724130518,-4.44704615044988,332.894915008386));
#42555=CARTESIAN_POINT('Ctrl Pts',(150.612066335054,-4.50170736277977,333.019138096082));
#42556=CARTESIAN_POINT('Ctrl Pts',(150.604408053322,-4.55637204609036,333.143369071929));
#42557=CARTESIAN_POINT('Ctrl Pts',(150.596749771589,-4.60588491556441,333.269852465188));
#42558=CARTESIAN_POINT('Ctrl Pts',(150.589091489856,-4.65006928660642,333.398114020206));
#42559=CARTESIAN_POINT('Ctrl Pts',(150.581378559544,-4.69456895201306,333.527290834275));
#42560=CARTESIAN_POINT('Ctrl Pts',(150.573665629233,-4.73366362839711,333.658270901046));
#42561=CARTESIAN_POINT('Ctrl Pts',(150.565952698921,-4.7672240071005,333.79055453673));
#42562=CARTESIAN_POINT('Ctrl Pts',(150.558284606373,-4.80058928844805,333.922069164776));
#42563=CARTESIAN_POINT('Ctrl Pts',(150.550616513825,-4.82848441999502,334.054871839774));
#42564=CARTESIAN_POINT('Ctrl Pts',(150.542948421276,-4.85083394677773,334.188462518864));
#42565=CARTESIAN_POINT('Ctrl Pts',(150.535213072083,-4.8733795006912,334.323224918401));
#42566=CARTESIAN_POINT('Ctrl Pts',(150.52747772289,-4.89028165472963,334.458788797211));
#42567=CARTESIAN_POINT('Ctrl Pts',(150.519742373697,-4.90151655350136,334.594637769085));
#42568=CARTESIAN_POINT('Ctrl Pts',(150.512007024504,-4.91275145227308,334.73048674096));
#42569=CARTESIAN_POINT('Ctrl Pts',(150.504271675311,-4.91831913794538,334.866620391478));
#42570=CARTESIAN_POINT('Ctrl Pts',(150.496536326118,-4.91824935158945,335.002525488068));
#42571=CARTESIAN_POINT('',(153.996536248542,-4.91824850103284,334.996160131745));
#42572=CARTESIAN_POINT('Ctrl Pts',(153.99653624849,-4.91824850103355,334.99616013266));
#42573=CARTESIAN_POINT('Ctrl Pts',(153.988795046099,-4.91835554475088,335.133265807329));
#42574=CARTESIAN_POINT('Ctrl Pts',(153.981053843708,-4.91272516499156,335.270440402459));
#42575=CARTESIAN_POINT('Ctrl Pts',(153.973312641316,-4.90136686420779,335.407168177718));
#42576=CARTESIAN_POINT('Ctrl Pts',(153.965572721839,-4.89001044578267,335.543873293714));
#42577=CARTESIAN_POINT('Ctrl Pts',(153.957832802361,-4.87292802653742,335.680131347521));
#42578=CARTESIAN_POINT('Ctrl Pts',(153.950092882884,-4.85018113288858,335.81542997288));
#42579=CARTESIAN_POINT('Ctrl Pts',(153.942352568803,-4.82743307953775,335.950735496152));
#42580=CARTESIAN_POINT('Ctrl Pts',(153.934612254722,-4.79902004156157,336.085081107864));
#42581=CARTESIAN_POINT('Ctrl Pts',(153.926871940641,-4.76505492617729,336.217963305282));
#42582=CARTESIAN_POINT('Ctrl Pts',(153.91912955453,-4.73108071856075,336.350881074368));
#42583=CARTESIAN_POINT('Ctrl Pts',(153.91138716842,-4.69155157263227,336.482334270744));
#42584=CARTESIAN_POINT('Ctrl Pts',(153.903644782309,-4.6466305397093,336.611833642142));
#42585=CARTESIAN_POINT('Ctrl Pts',(153.895893585931,-4.60165838994896,336.741480374317));
#42586=CARTESIAN_POINT('Ctrl Pts',(153.888142389554,-4.55128222528017,336.869168470188));
#42587=CARTESIAN_POINT('Ctrl Pts',(153.880391193176,-4.49571385557278,336.994427233897));
#42588=CARTESIAN_POINT('Ctrl Pts',(153.872635568759,-4.44011374122829,337.119757554393));
#42589=CARTESIAN_POINT('Ctrl Pts',(153.864879944342,-4.37931568542567,337.242655427412));
#42590=CARTESIAN_POINT('Ctrl Pts',(153.857124319926,-4.3135774697723,337.362674855915));
#42591=CARTESIAN_POINT('Ctrl Pts',(153.849355638484,-4.24772858018298,337.48289634379));
#42592=CARTESIAN_POINT('Ctrl Pts',(153.841586957043,-4.17692311280368,337.600229368254));
#42593=CARTESIAN_POINT('Ctrl Pts',(153.833818275602,-4.10146269925848,337.714256212868));
#42594=CARTESIAN_POINT('Ctrl Pts',(153.826141221996,-4.02689230473695,337.826938166085));
#42595=CARTESIAN_POINT('Ctrl Pts',(153.818464168389,-3.94777646187569,337.936391269431));
#42596=CARTESIAN_POINT('Ctrl Pts',(153.810787114782,-3.86444337650643,338.042245955257));
#42597=CARTESIAN_POINT('Ctrl Pts',(153.803012036004,-3.78004624490054,338.149452256465));
#42598=CARTESIAN_POINT('Ctrl Pts',(153.795236957225,-3.69105123874667,338.253313320985));
#42599=CARTESIAN_POINT('Ctrl Pts',(153.787461878447,-3.59775322759171,338.353409425622));
#42600=CARTESIAN_POINT('Ctrl Pts',(153.779696367398,-3.50457002557909,338.453382355631));
#42601=CARTESIAN_POINT('Ctrl Pts',(153.771930856349,-3.40709461830108,338.54959926095));
#42602=CARTESIAN_POINT('Ctrl Pts',(153.7641653453,-3.30566348531353,338.641671592053));
#42603=CARTESIAN_POINT('Ctrl Pts',(153.756407533778,-3.20433292158963,338.733652633171));
#42604=CARTESIAN_POINT('Ctrl Pts',(153.748649722255,-3.09905472493873,338.821497016904));
#42605=CARTESIAN_POINT('Ctrl Pts',(153.740891910733,-2.99020350399843,338.904851606294));
#42606=CARTESIAN_POINT('Ctrl Pts',(153.73313993721,-2.88143419705372,338.988143468712));
#42607=CARTESIAN_POINT('Ctrl Pts',(153.725387963687,-2.76909752685823,339.066952025261));
#42608=CARTESIAN_POINT('Ctrl Pts',(153.717635990164,-2.6536023146422,339.140963392524));
#42609=CARTESIAN_POINT('Ctrl Pts',(153.709887299606,-2.53815601471722,339.214943415929));
#42610=CARTESIAN_POINT('Ctrl Pts',(153.702138609049,-2.41955416166732,339.284130080327));
#42611=CARTESIAN_POINT('Ctrl Pts',(153.694389918491,-2.29823560290742,339.348252082852));
#42612=CARTESIAN_POINT('Ctrl Pts',(153.686642840113,-2.17694228548709,339.412360744259));
#42613=CARTESIAN_POINT('Ctrl Pts',(153.678895761736,-2.05293373200298,339.47140665723));
#42614=CARTESIAN_POINT('Ctrl Pts',(153.671148683358,-1.92667415244975,339.525164060317));
#42615=CARTESIAN_POINT('Ctrl Pts',(153.663401540052,-1.80041351471949,339.578921913942));
#42616=CARTESIAN_POINT('Ctrl Pts',(153.655654396746,-1.671902172925,339.627391016158));
#42617=CARTESIAN_POINT('Ctrl Pts',(153.64790725344,-1.54162474196582,339.670393582714));
#42618=CARTESIAN_POINT('Ctrl Pts',(153.640158368412,-1.41131802187474,339.713405817161));
#42619=CARTESIAN_POINT('Ctrl Pts',(153.632409483384,-1.27924479362876,339.750948947894));
#42620=CARTESIAN_POINT('Ctrl Pts',(153.624660598356,-1.14590488371914,339.782895050068));
#42621=CARTESIAN_POINT('Ctrl Pts',(153.616903488581,-1.01242344545098,339.814875060166));
#42622=CARTESIAN_POINT('Ctrl Pts',(153.609146378807,-0.877673020533642,
339.841246083298));
#42623=CARTESIAN_POINT('Ctrl Pts',(153.601389269032,-0.742164230805109,
339.861931233267));
#42624=CARTESIAN_POINT('Ctrl Pts',(153.593628014106,-0.606583029512098,
339.882627436718));
#42625=CARTESIAN_POINT('Ctrl Pts',(153.58586675918,-0.470243044250462,339.897631670086));
#42626=CARTESIAN_POINT('Ctrl Pts',(153.578105504253,-0.333659083452315,
339.906919061746));
#42627=CARTESIAN_POINT('Ctrl Pts',(153.570331833849,-0.196856632829616,
339.916221310207));
#42628=CARTESIAN_POINT('Ctrl Pts',(153.562558163444,-0.0598098177201696,
339.9197884322));
#42629=CARTESIAN_POINT('Ctrl Pts',(153.554784493039,0.0769665939859852,
339.91764773097));
#42630=CARTESIAN_POINT('Ctrl Pts',(153.547372688862,0.207376030821223,339.915606679897));
#42631=CARTESIAN_POINT('Ctrl Pts',(153.539960884685,0.337539384918909,339.908377261115));
#42632=CARTESIAN_POINT('Ctrl Pts',(153.532549080508,0.467017474504463,339.896026730014));
#42633=CARTESIAN_POINT('Ctrl Pts',(153.52477400173,0.602841670955703,339.883070862593));
#42634=CARTESIAN_POINT('Ctrl Pts',(153.516998922951,0.738340960250965,339.864438244851));
#42635=CARTESIAN_POINT('Ctrl Pts',(153.509223844173,0.873002817372639,339.840149702577));
#42636=CARTESIAN_POINT('Ctrl Pts',(153.501458333124,1.00749896450609,339.815891048902));
#42637=CARTESIAN_POINT('Ctrl Pts',(153.493692822075,1.14115934890247,339.785990387768));
#42638=CARTESIAN_POINT('Ctrl Pts',(153.485927311026,1.27347514258071,339.750520405569));
#42639=CARTESIAN_POINT('Ctrl Pts',(153.478169499503,1.40565974476388,339.715085591961));
#42640=CARTESIAN_POINT('Ctrl Pts',(153.470411687981,1.5365020341918,339.674092546933));
#42641=CARTESIAN_POINT('Ctrl Pts',(153.462653876459,1.66550232823403,339.62766518421));
#42642=CARTESIAN_POINT('Ctrl Pts',(153.454901902936,1.79440554546437,339.581272759549));
#42643=CARTESIAN_POINT('Ctrl Pts',(153.447149929413,1.9214691600932,339.529454288967));
#42644=CARTESIAN_POINT('Ctrl Pts',(153.43939795589,2.04620798423178,339.472383698629));
#42645=CARTESIAN_POINT('Ctrl Pts',(153.431649265332,2.17089398140445,339.415337277721));
#42646=CARTESIAN_POINT('Ctrl Pts',(153.423900574775,2.29325679158807,339.353043323267));
#42647=CARTESIAN_POINT('Ctrl Pts',(153.416151884217,2.41283078489675,339.285724053874));
#42648=CARTESIAN_POINT('Ctrl Pts',(153.408404805839,2.53237989983724,339.218418790817));
#42649=CARTESIAN_POINT('Ctrl Pts',(153.400657727461,2.64914101164359,339.146090484148));
#42650=CARTESIAN_POINT('Ctrl Pts',(153.392910649084,2.7626730620327,339.069007325481));
#42651=CARTESIAN_POINT('Ctrl Pts',(153.385163505778,2.87620606392955,338.991923520783));
#42652=CARTESIAN_POINT('Ctrl Pts',(153.377416362472,2.98650962704934,338.910085004164));
#42653=CARTESIAN_POINT('Ctrl Pts',(153.369669219166,3.09317199589559,338.823803089374));
#42654=CARTESIAN_POINT('Ctrl Pts',(153.361920334138,3.19985834470723,338.737501776578));
#42655=CARTESIAN_POINT('Ctrl Pts',(153.35417144911,3.30290156645283,338.64675532355));
#42656=CARTESIAN_POINT('Ctrl Pts',(153.346422564082,3.40192360160668,338.551914817578));
#42657=CARTESIAN_POINT('Ctrl Pts',(153.338665454307,3.50105073977157,338.456973646913));
#42658=CARTESIAN_POINT('Ctrl Pts',(153.330908344532,3.59614788262497,338.357930013612));
#42659=CARTESIAN_POINT('Ctrl Pts',(153.323151234758,3.6868740481465,338.255171702937));
#42660=CARTESIAN_POINT('Ctrl Pts',(153.315389979832,3.77764869483008,338.152358481507));
#42661=CARTESIAN_POINT('Ctrl Pts',(153.307628724905,3.86404746398213,338.045826930833));
#42662=CARTESIAN_POINT('Ctrl Pts',(153.299867469979,3.94577084814139,337.935996504844));
#42663=CARTESIAN_POINT('Ctrl Pts',(153.292093799574,4.02762496308171,337.825990385968));
#42664=CARTESIAN_POINT('Ctrl Pts',(153.28432012917,4.10478852746684,337.712675169768));
#42665=CARTESIAN_POINT('Ctrl Pts',(153.276546458765,4.1770059307357,337.596498510899));
#42666=CARTESIAN_POINT('Ctrl Pts',(153.269134654588,4.24586159650712,337.485729903451));
#42667=CARTESIAN_POINT('Ctrl Pts',(153.261722850411,4.31022108369358,337.372360508752));
#42668=CARTESIAN_POINT('Ctrl Pts',(153.254311046234,4.36990328232864,337.256796039875));
#42669=CARTESIAN_POINT('Ctrl Pts',(153.246535967456,4.43251068330356,337.135567412128));
#42670=CARTESIAN_POINT('Ctrl Pts',(153.238760888677,4.49016855791999,337.011539990409));
#42671=CARTESIAN_POINT('Ctrl Pts',(153.230985809899,4.54261706233336,336.885156037971));
#42672=CARTESIAN_POINT('Ctrl Pts',(153.22322029885,4.5950010255231,336.758927609032));
#42673=CARTESIAN_POINT('Ctrl Pts',(153.215454787801,4.64218822510127,336.630348776834));
#42674=CARTESIAN_POINT('Ctrl Pts',(153.207689276752,4.68396442858952,336.499886760462));
#42675=CARTESIAN_POINT('Ctrl Pts',(153.19993146523,4.72569921085014,336.369554097559));
#42676=CARTESIAN_POINT('Ctrl Pts',(153.192173653707,4.76203355527629,336.237342336136));
#42677=CARTESIAN_POINT('Ctrl Pts',(153.184415842185,4.79280125661933,336.103738726805));
#42678=CARTESIAN_POINT('Ctrl Pts',(153.176663868662,4.82354580429143,335.970235658426));
#42679=CARTESIAN_POINT('Ctrl Pts',(153.168911895139,4.84873195966467,335.835343206326));
#42680=CARTESIAN_POINT('Ctrl Pts',(153.161159921616,4.86824341795597,335.699563496781));
#42681=CARTESIAN_POINT('Ctrl Pts',(153.153411231059,4.88774661313315,335.563841290023));
#42682=CARTESIAN_POINT('Ctrl Pts',(153.145662540501,4.90157983561699,335.427232959263));
#42683=CARTESIAN_POINT('Ctrl Pts',(153.137913849943,4.90967797472423,335.290250317843));
#42684=CARTESIAN_POINT('Ctrl Pts',(153.130166771566,4.91777442894599,335.153296176805));
#42685=CARTESIAN_POINT('Ctrl Pts',(153.122419693188,4.92013815016103,335.015968269962));
#42686=CARTESIAN_POINT('Ctrl Pts',(153.11467261481,4.9167559844742,334.878782626505));
#42687=CARTESIAN_POINT('Ctrl Pts',(153.106925471504,4.91337379044156,334.741595833299));
#42688=CARTESIAN_POINT('Ctrl Pts',(153.099178328198,4.9042456230898,334.604551696612));
#42689=CARTESIAN_POINT('Ctrl Pts',(153.091431184892,4.88941044826714,334.468164940159));
#42690=CARTESIAN_POINT('Ctrl Pts',(153.083682299864,4.87457193818225,334.331747521068));
#42691=CARTESIAN_POINT('Ctrl Pts',(153.075933414836,4.85402390974645,334.195988164808));
#42692=CARTESIAN_POINT('Ctrl Pts',(153.068184529808,4.82785701004614,334.061394783176));
#42693=CARTESIAN_POINT('Ctrl Pts',(153.060427420033,4.80166233652811,333.926658542739));
#42694=CARTESIAN_POINT('Ctrl Pts',(153.052670310259,4.76983695295263,333.793091133403));
#42695=CARTESIAN_POINT('Ctrl Pts',(153.044913200484,4.73252243128416,333.661189147082));
#42696=CARTESIAN_POINT('Ctrl Pts',(153.037151945558,4.69518796992836,333.529216676556));
#42697=CARTESIAN_POINT('Ctrl Pts',(153.029390690632,4.65235864776371,333.39891177349));
#42698=CARTESIAN_POINT('Ctrl Pts',(153.021629435705,4.60422511187629,333.270753290688));
#42699=CARTESIAN_POINT('Ctrl Pts',(153.013855765301,4.55601457801818,333.14238979608));
#42700=CARTESIAN_POINT('Ctrl Pts',(153.006082094896,4.50248302757505,333.016179943064));
#42701=CARTESIAN_POINT('Ctrl Pts',(152.998308424491,4.44386857735386,332.892580931635));
#42702=CARTESIAN_POINT('Ctrl Pts',(152.990896620314,4.38798264389175,332.774735483923));
#42703=CARTESIAN_POINT('Ctrl Pts',(152.983484816137,4.32747651272099,332.65926353349));
#42704=CARTESIAN_POINT('Ctrl Pts',(152.97607301196,4.26259334762634,332.546536934194));
#42705=CARTESIAN_POINT('Ctrl Pts',(152.968297933181,4.19453006533398,332.428285268473));
#42706=CARTESIAN_POINT('Ctrl Pts',(152.960522854403,4.12143474476487,332.312681177048));
#42707=CARTESIAN_POINT('Ctrl Pts',(152.952747775625,4.04353867810841,332.200182502172));
#42708=CARTESIAN_POINT('Ctrl Pts',(152.944982264576,3.96573846752111,332.087822264079));
#42709=CARTESIAN_POINT('Ctrl Pts',(152.937216753527,3.88314948570998,331.978560157305));
#42710=CARTESIAN_POINT('Ctrl Pts',(152.929451242478,3.7960486936827,331.872829173568));
#42711=CARTESIAN_POINT('Ctrl Pts',(152.921693430955,3.70903426234456,331.767203022409));
#42712=CARTESIAN_POINT('Ctrl Pts',(152.913935619433,3.61751717018306,331.665101326606));
#42713=CARTESIAN_POINT('Ctrl Pts',(152.906177807911,3.52181721343487,331.566927530964));
#42714=CARTESIAN_POINT('Ctrl Pts',(152.898425834388,3.42618927393833,331.468827614215));
#42715=CARTESIAN_POINT('Ctrl Pts',(152.890673860865,3.32638500701644,331.37464999288));
#42716=CARTESIAN_POINT('Ctrl Pts',(152.882921887342,3.22276372217456,331.284764199471));
#42717=CARTESIAN_POINT('Ctrl Pts',(152.875173196784,3.11918632100873,331.194916472748));
#42718=CARTESIAN_POINT('Ctrl Pts',(152.867424506227,3.01179541169728,331.109357214484));
#42719=CARTESIAN_POINT('Ctrl Pts',(152.859675815669,2.90098615387256,331.028418149208));
#42720=CARTESIAN_POINT('Ctrl Pts',(152.851928737291,2.79019995083955,330.947495923981));
#42721=CARTESIAN_POINT('Ctrl Pts',(152.844181658913,2.67599712939249,330.871192210117));
#42722=CARTESIAN_POINT('Ctrl Pts',(152.836434580535,2.55880451115963,330.799797322013));
#42723=CARTESIAN_POINT('Ctrl Pts',(152.82868743723,2.44161091073966,330.728401835551));
#42724=CARTESIAN_POINT('Ctrl Pts',(152.820940293924,2.32142779736306,330.661915460266));
#42725=CARTESIAN_POINT('Ctrl Pts',(152.813193150618,2.19870909983899,330.600583975482));
#42726=CARTESIAN_POINT('Ctrl Pts',(152.80544426559,2.07596281254593,330.539238702078));
#42727=CARTESIAN_POINT('Ctrl Pts',(152.797695380562,1.95068015633531,330.48305080002));
#42728=CARTESIAN_POINT('Ctrl Pts',(152.789946495534,1.82333729941243,330.432218902457));
#42729=CARTESIAN_POINT('Ctrl Pts',(152.782189385759,1.695859279466,330.381333051393));
#42730=CARTESIAN_POINT('Ctrl Pts',(152.774432275984,1.56631705422675,330.335814706118));
#42731=CARTESIAN_POINT('Ctrl Pts',(152.766675166209,1.43520483114177,330.295813550127));
#42732=CARTESIAN_POINT('Ctrl Pts',(152.758913911283,1.304022545877,330.255791018797));
#42733=CARTESIAN_POINT('Ctrl Pts',(152.751152656357,1.17126896918634,330.221291649586));
#42734=CARTESIAN_POINT('Ctrl Pts',(152.743391401431,1.03744994868626,330.192414258022));
#42735=CARTESIAN_POINT('Ctrl Pts',(152.735617731026,0.903416861364845,330.163490672042));
#42736=CARTESIAN_POINT('Ctrl Pts',(152.727844060621,0.76831530981056,330.140207101469));
#42737=CARTESIAN_POINT('Ctrl Pts',(152.720070390217,0.632658621919278,330.122610725951));
#42738=CARTESIAN_POINT('Ctrl Pts',(152.71265858604,0.503316785489045,330.105833465946));
#42739=CARTESIAN_POINT('Ctrl Pts',(152.705246781863,0.373470619469935,330.094225864332));
#42740=CARTESIAN_POINT('Ctrl Pts',(152.697834977686,0.243564413581649,330.087784670952));
#42741=CARTESIAN_POINT('Ctrl Pts',(152.690059898908,0.107291117569584,330.081027775497));
#42742=CARTESIAN_POINT('Ctrl Pts',(152.682284820129,-0.0294789013836393,
330.079935182752));
#42743=CARTESIAN_POINT('Ctrl Pts',(152.674509741351,-0.16623546848306,330.084560158895));
#42744=CARTESIAN_POINT('Ctrl Pts',(152.666744230302,-0.3028237479202,330.089179443711));
#42745=CARTESIAN_POINT('Ctrl Pts',(152.658978719253,-0.439398221523491,
330.099502285041));
#42746=CARTESIAN_POINT('Ctrl Pts',(152.651213208204,-0.575444897828011,
330.115530097128));
#42747=CARTESIAN_POINT('Ctrl Pts',(152.643455396681,-0.71135668345707,330.131542017592));
#42748=CARTESIAN_POINT('Ctrl Pts',(152.635697585159,-0.846741327519914,
330.15324760663));
#42749=CARTESIAN_POINT('Ctrl Pts',(152.627939773637,-0.981086504580793,
330.180596267895));
#42750=CARTESIAN_POINT('Ctrl Pts',(152.620187800114,-1.11533058263551,330.207924348425));
#42751=CARTESIAN_POINT('Ctrl Pts',(152.612435826591,-1.24853636920625,330.240886970895));
#42752=CARTESIAN_POINT('Ctrl Pts',(152.604683853068,-1.38019867352889,330.279381959522));
#42753=CARTESIAN_POINT('Ctrl Pts',(152.59693516251,-1.51180521878738,330.317860645498));
#42754=CARTESIAN_POINT('Ctrl Pts',(152.589186471953,-1.64186920750584,330.361866928186));
#42755=CARTESIAN_POINT('Ctrl Pts',(152.581437781395,-1.76989784189834,330.411248024599));
#42756=CARTESIAN_POINT('Ctrl Pts',(152.573690703017,-1.89789983886424,330.460618846863));
#42757=CARTESIAN_POINT('Ctrl Pts',(152.565943624639,-2.02386695936215,330.51536211795));
#42758=CARTESIAN_POINT('Ctrl Pts',(152.558196546262,-2.14732409414879,330.575276020226));
#42759=CARTESIAN_POINT('Ctrl Pts',(152.550449402956,-2.27078226362516,330.635190424638));
#42760=CARTESIAN_POINT('Ctrl Pts',(152.54270225965,-2.39173005378051,330.700275376016));
#42761=CARTESIAN_POINT('Ctrl Pts',(152.534955116344,-2.50971513661294,330.770282161236));
#42762=CARTESIAN_POINT('Ctrl Pts',(152.527206231316,-2.62772674499622,330.840304685467));
#42763=CARTESIAN_POINT('Ctrl Pts',(152.519457346288,-2.74277398454481,330.915251045998));
#42764=CARTESIAN_POINT('Ctrl Pts',(152.51170846126,-2.85443213846829,330.994828314619));
#42765=CARTESIAN_POINT('Ctrl Pts',(152.503951351485,-2.96620880751044,331.074490047375));
#42766=CARTESIAN_POINT('Ctrl Pts',(152.496194241711,-3.07458888635121,331.158792279771));
#42767=CARTESIAN_POINT('Ctrl Pts',(152.488437131936,-3.17917905894054,331.247400424546));
#42768=CARTESIAN_POINT('Ctrl Pts',(152.48067587701,-3.28382512117416,331.336055918682));
#42769=CARTESIAN_POINT('Ctrl Pts',(152.472914622083,-3.38467695450139,331.429021645241));
#42770=CARTESIAN_POINT('Ctrl Pts',(152.465153367157,-3.48137771966674,331.525925700923));
#42771=CARTESIAN_POINT('Ctrl Pts',(152.457379696753,-3.57823317454143,331.622984771513));
#42772=CARTESIAN_POINT('Ctrl Pts',(152.449606026348,-3.67092402744085,331.723994472432));
#42773=CARTESIAN_POINT('Ctrl Pts',(152.441832355943,-3.75913281281358,331.828548666915));
#42774=CARTESIAN_POINT('Ctrl Pts',(152.434420551766,-3.84323545800619,331.928235838491));
#42775=CARTESIAN_POINT('Ctrl Pts',(152.427008747589,-3.92326374884816,332.031144710368));
#42776=CARTESIAN_POINT('Ctrl Pts',(152.419596943412,-3.99897998780284,332.136899910996));
#42777=CARTESIAN_POINT('Ctrl Pts',(152.411752387183,-4.07911706101047,332.248829826849));
#42778=CARTESIAN_POINT('Ctrl Pts',(152.403907830954,-4.15467548780588,332.364300171864));
#42779=CARTESIAN_POINT('Ctrl Pts',(152.396063274724,-4.22532975812652,332.482904154071));
#42780=CARTESIAN_POINT('Ctrl Pts',(152.388228710807,-4.29589402979664,332.6013570598));
#42781=CARTESIAN_POINT('Ctrl Pts',(152.380394146889,-4.36156638223422,332.722935335455));
#42782=CARTESIAN_POINT('Ctrl Pts',(152.372559582971,-4.4220627456671,332.847200860302));
#42783=CARTESIAN_POINT('Ctrl Pts',(152.364733405835,-4.48249434866032,332.971333360789));
#42784=CARTESIAN_POINT('Ctrl Pts',(152.356907228699,-4.53776082443947,333.098147044492));
#42785=CARTESIAN_POINT('Ctrl Pts',(152.349081051563,-4.58762262067717,333.227176897502));
#42786=CARTESIAN_POINT('Ctrl Pts',(152.341261661756,-4.63744117378289,333.356094848106));
#42787=CARTESIAN_POINT('Ctrl Pts',(152.333442271949,-4.6818642413228,333.487224787547));
#42788=CARTESIAN_POINT('Ctrl Pts',(152.325622882142,-4.72069937701304,333.620079547811));
#42789=CARTESIAN_POINT('Ctrl Pts',(152.31780913696,-4.7595064785793,333.75283840351));
#42790=CARTESIAN_POINT('Ctrl Pts',(152.309995391777,-4.79273357672973,333.887319234516));
#42791=CARTESIAN_POINT('Ctrl Pts',(152.302181646594,-4.8202374249548,334.023017794653));
#42792=CARTESIAN_POINT('Ctrl Pts',(152.294371178942,-4.84772973649703,334.158659435073));
#42793=CARTESIAN_POINT('Ctrl Pts',(152.286560711289,-4.86950350289265,334.295517414046));
#42794=CARTESIAN_POINT('Ctrl Pts',(152.278750243637,-4.8854661601859,334.43307543696));
#42795=CARTESIAN_POINT('Ctrl Pts',(152.27094092684,-4.9014264654151,334.570613190987));
#42796=CARTESIAN_POINT('Ctrl Pts',(152.263131610044,-4.91157732054033,334.708850404923));
#42797=CARTESIAN_POINT('Ctrl Pts',(152.255322293248,-4.91587782163216,334.847263935873));
#42798=CARTESIAN_POINT('Ctrl Pts',(152.252393611662,-4.91749061295388,334.899172338349));
#42799=CARTESIAN_POINT('Ctrl Pts',(152.249464930076,-4.91828111641089,334.951105496473));
#42800=CARTESIAN_POINT('Ctrl Pts',(152.24653624849,-4.91824906311716,335.003035728436));
#42801=CARTESIAN_POINT('',(155.746536248441,-4.91824983112492,334.998711147934));
#42802=CARTESIAN_POINT('Ctrl Pts',(155.746536248441,-4.91824983112492,334.998711147934));
#42803=CARTESIAN_POINT('Ctrl Pts',(155.73881437765,-4.91828535226794,335.134259563696));
#42804=CARTESIAN_POINT('Ctrl Pts',(155.731092506859,-4.91271300065732,335.270034172756));
#42805=CARTESIAN_POINT('Ctrl Pts',(155.723370636069,-4.90150278861575,335.405528637327));
#42806=CARTESIAN_POINT('Ctrl Pts',(155.715658110667,-4.89030614372606,335.540859119809));
#42807=CARTESIAN_POINT('Ctrl Pts',(155.707945585266,-4.87348524360162,335.675909740718));
#42808=CARTESIAN_POINT('Ctrl Pts',(155.700233059864,-4.85106207896362,335.810172678224));
#42809=CARTESIAN_POINT('Ctrl Pts',(155.692527960626,-4.8286605049299,335.944306337906));
#42810=CARTESIAN_POINT('Ctrl Pts',(155.684822861388,-4.80066746362549,336.07765343435));
#42811=CARTESIAN_POINT('Ctrl Pts',(155.67711776215,-4.76715682936312,336.209710224292));
#42812=CARTESIAN_POINT('Ctrl Pts',(155.669418176934,-4.73367017641276,336.341672510052));
#42813=CARTESIAN_POINT('Ctrl Pts',(155.661718591718,-4.69467388546408,336.472345943801));
#42814=CARTESIAN_POINT('Ctrl Pts',(155.654019006503,-4.65029301382672,336.601236381068));
#42815=CARTESIAN_POINT('Ctrl Pts',(155.646322237362,-4.60592837421368,336.730079677468));
#42816=CARTESIAN_POINT('Ctrl Pts',(155.638625468221,-4.55618319763893,336.857140899253));
#42817=CARTESIAN_POINT('Ctrl Pts',(155.63092869908,-4.50123248290631,336.981940765343));
#42818=CARTESIAN_POINT('Ctrl Pts',(155.623233156016,-4.44629052169457,337.106720751105));
#42819=CARTESIAN_POINT('Ctrl Pts',(155.615537612953,-4.38614483115809,337.229239734583));
#42820=CARTESIAN_POINT('Ctrl Pts',(155.607842069889,-4.32101847795669,337.349038606677));
#42821=CARTESIAN_POINT('Ctrl Pts',(155.600146030071,-4.25588792078289,337.46884521191));
#42822=CARTESIAN_POINT('Ctrl Pts',(155.592449990252,-4.1857762509565,337.585931007953));
#42823=CARTESIAN_POINT('Ctrl Pts',(155.584753950433,-4.1109521632586,337.699862102756));
#42824=CARTESIAN_POINT('Ctrl Pts',(155.577055690991,-4.03610649546407,337.813826056551));
#42825=CARTESIAN_POINT('Ctrl Pts',(155.56935743155,-3.9565459240256,337.924633167845));
#42826=CARTESIAN_POINT('Ctrl Pts',(155.561659172108,-3.87258179019653,338.031879506303));
#42827=CARTESIAN_POINT('Ctrl Pts',(155.553952605069,-3.78852704625478,338.139241579925));
#42828=CARTESIAN_POINT('Ctrl Pts',(155.546246038031,-3.70005949677172,338.243034896075));
#42829=CARTESIAN_POINT('Ctrl Pts',(155.538539470992,-3.60753024948391,338.342889253559));
#42830=CARTESIAN_POINT('Ctrl Pts',(155.530828242175,-3.51494503033456,338.442804013936));
#42831=CARTESIAN_POINT('Ctrl Pts',(155.523117013357,-3.41829350140623,338.538774791744));
#42832=CARTESIAN_POINT('Ctrl Pts',(155.51540578454,-3.31796190590271,338.630469921853));
#42833=CARTESIAN_POINT('Ctrl Pts',(155.507683202205,-3.2174825886095,338.722300057975));
#42834=CARTESIAN_POINT('Ctrl Pts',(155.49996061987,-3.11331268921402,338.809841722717));
#42835=CARTESIAN_POINT('Ctrl Pts',(155.492238037535,-3.00587000081113,338.892804721627));
#42836=CARTESIAN_POINT('Ctrl Pts',(155.488230465165,-2.95011347654464,338.935857706718));
#42837=CARTESIAN_POINT('Ctrl Pts',(155.484222892795,-2.8934760464137,338.977678378518));
#42838=CARTESIAN_POINT('Ctrl Pts',(155.480215320426,-2.83601879579477,339.018231010333));
#42839=CARTESIAN_POINT('Ctrl Pts',(155.472440241647,-2.72454616130369,339.096907046086));
#42840=CARTESIAN_POINT('Ctrl Pts',(155.464665162869,-2.60962098522146,339.171065226659));
#42841=CARTESIAN_POINT('Ctrl Pts',(155.45689008409,-2.49164561765528,339.240387385431));
#42842=CARTESIAN_POINT('Ctrl Pts',(155.449124573041,-2.37381542628964,339.309624238873));
#42843=CARTESIAN_POINT('Ctrl Pts',(155.441359061992,-2.25294284551895,339.374036715234));
#42844=CARTESIAN_POINT('Ctrl Pts',(155.433593550943,-2.12946121369527,339.433348396175));
#42845=CARTESIAN_POINT('Ctrl Pts',(155.425835739421,-2.0061020142688,339.492601269411));
#42846=CARTESIAN_POINT('Ctrl Pts',(155.418077927899,-1.88013926189763,339.546763243698));
#42847=CARTESIAN_POINT('Ctrl Pts',(155.410320116377,-1.75203273767333,339.595602718754));
#42848=CARTESIAN_POINT('Ctrl Pts',(155.402568142854,-1.62402261767111,339.644405440557));
#42849=CARTESIAN_POINT('Ctrl Pts',(155.394816169331,-1.4938723006851,339.6878934969));
#42850=CARTESIAN_POINT('Ctrl Pts',(155.387064195808,-1.36206316109458,339.725882669691));
#42851=CARTESIAN_POINT('Ctrl Pts',(155.37931550525,-1.23030984275312,339.763855754046));
#42852=CARTESIAN_POINT('Ctrl Pts',(155.371566814692,-1.09689947385912,339.796334478605));
#42853=CARTESIAN_POINT('Ctrl Pts',(155.363818124135,-0.962330060539396,
339.823184001993));
#42854=CARTESIAN_POINT('Ctrl Pts',(155.356071045757,-0.827788645510108,
339.850027939114));
#42855=CARTESIAN_POINT('Ctrl Pts',(155.348323967379,-0.6920890487956,339.871244928235));
#42856=CARTESIAN_POINT('Ctrl Pts',(155.340576889001,-0.555740593810602,
339.886751012165));
#42857=CARTESIAN_POINT('Ctrl Pts',(155.332829745696,-0.419390996094409,
339.90225722605));
#42858=CARTESIAN_POINT('Ctrl Pts',(155.32508260239,-0.282392917632038,339.912052395111));
#42859=CARTESIAN_POINT('Ctrl Pts',(155.317335459084,-0.145261552604407,
339.916104366654));
#42860=CARTESIAN_POINT('Ctrl Pts',(155.309586574056,-0.00809935753444271,
339.920157249166));
#42861=CARTESIAN_POINT('Ctrl Pts',(155.301837689028,0.129195793101662,339.918464353288));
#42862=CARTESIAN_POINT('Ctrl Pts',(155.294088804,0.266108348808019,339.911045653341));
#42863=CARTESIAN_POINT('Ctrl Pts',(155.286331694225,0.40316622491569,339.903619079108));
#42864=CARTESIAN_POINT('Ctrl Pts',(155.27857458445,0.539840303972119,339.890454581757));
#42865=CARTESIAN_POINT('Ctrl Pts',(155.270817474676,0.675619248307293,339.87162413306));
#42866=CARTESIAN_POINT('Ctrl Pts',(155.263056219749,0.811470748569065,339.852783621974));
#42867=CARTESIAN_POINT('Ctrl Pts',(155.255294964823,0.946425776604411,339.828271196388));
#42868=CARTESIAN_POINT('Ctrl Pts',(155.247533709897,1.07998382011621,339.79820987565));
#42869=CARTESIAN_POINT('Ctrl Pts',(155.239760039492,1.21375551297109,339.768100466596));
#42870=CARTESIAN_POINT('Ctrl Pts',(155.231986369088,1.34612537806441,339.732424526438));
#42871=CARTESIAN_POINT('Ctrl Pts',(155.224212698683,1.47660782568998,339.691355069872));
#42872=CARTESIAN_POINT('Ctrl Pts',(155.216800894506,1.60101628398516,339.65219740639));
#42873=CARTESIAN_POINT('Ctrl Pts',(155.209389090329,1.72370881808154,339.60813715988));
#42874=CARTESIAN_POINT('Ctrl Pts',(155.201977286152,1.84428368065753,339.55936407493));
#42875=CARTESIAN_POINT('Ctrl Pts',(155.194202207374,1.97076827642355,339.508200475798));
#42876=CARTESIAN_POINT('Ctrl Pts',(155.186427128595,2.09532207974599,339.451688690113));
#42877=CARTESIAN_POINT('Ctrl Pts',(155.178652049817,2.21745980279598,339.389994884449));
#42878=CARTESIAN_POINT('Ctrl Pts',(155.170886538768,2.3394472276023,339.32837699694));
#42879=CARTESIAN_POINT('Ctrl Pts',(155.163121027719,2.45902414227711,339.261589952012));
#42880=CARTESIAN_POINT('Ctrl Pts',(155.15535551667,2.57572359649386,339.189848567307));
#42881=CARTESIAN_POINT('Ctrl Pts',(155.147597705147,2.69230734286179,339.118178314394));
#42882=CARTESIAN_POINT('Ctrl Pts',(155.139839893625,2.8060189755836,339.041563700727));
#42883=CARTESIAN_POINT('Ctrl Pts',(155.132082082103,2.91641492311124,338.960266033836));
#42884=CARTESIAN_POINT('Ctrl Pts',(155.12433010858,3.02672779418749,338.879029546017));
#42885=CARTESIAN_POINT('Ctrl Pts',(155.116578135057,3.13372963308817,338.79311725046));
#42886=CARTESIAN_POINT('Ctrl Pts',(155.108826161534,3.23700502759131,338.702834254169));
#42887=CARTESIAN_POINT('Ctrl Pts',(155.101077470976,3.3402366849036,338.612589492781));
#42888=CARTESIAN_POINT('Ctrl Pts',(155.093328780419,3.43974474298275,338.517977968881));
#42889=CARTESIAN_POINT('Ctrl Pts',(155.085580089861,3.53514631114801,338.419345496038));
#42890=CARTESIAN_POINT('Ctrl Pts',(155.077833011483,3.6305280302202,338.320733544505));
#42891=CARTESIAN_POINT('Ctrl Pts',(155.070085933105,3.72180468724035,338.218102588848));
#42892=CARTESIAN_POINT('Ctrl Pts',(155.062338854728,3.8086300566899,338.111835495938));
#42893=CARTESIAN_POINT('Ctrl Pts',(155.054591711422,3.89545615381955,338.005567512407));
#42894=CARTESIAN_POINT('Ctrl Pts',(155.046844568116,3.97783064165802,337.895663633528));
#42895=CARTESIAN_POINT('Ctrl Pts',(155.03909742481,4.05544768118593,337.78253969741));
#42896=CARTESIAN_POINT('Ctrl Pts',(155.031348539782,4.13308217067191,337.669390328631));
#42897=CARTESIAN_POINT('Ctrl Pts',(155.023599654754,4.20595686241477,337.5530197843));
#42898=CARTESIAN_POINT('Ctrl Pts',(155.015850769726,4.27380955929132,337.433872411079));
#42899=CARTESIAN_POINT('Ctrl Pts',(155.008093659951,4.34173427572167,337.314598573604));
#42900=CARTESIAN_POINT('Ctrl Pts',(155.000336550176,4.40462615558138,337.192542359817));
#42901=CARTESIAN_POINT('Ctrl Pts',(154.992579440402,4.46226900731624,337.068172712528));
#42902=CARTESIAN_POINT('Ctrl Pts',(154.984818185476,4.51994266154805,336.943736606076));
#42903=CARTESIAN_POINT('Ctrl Pts',(154.977056930549,4.57236154931104,336.816984963854));
#42904=CARTESIAN_POINT('Ctrl Pts',(154.969295675623,4.61935826427569,336.68840525016));
#42905=CARTESIAN_POINT('Ctrl Pts',(154.961522005219,4.66643015866804,336.559619850828));
#42906=CARTESIAN_POINT('Ctrl Pts',(154.953748334814,4.70806242885946,336.429000908979));
#42907=CARTESIAN_POINT('Ctrl Pts',(154.945974664409,4.74413778614593,336.297050395537));
#42908=CARTESIAN_POINT('Ctrl Pts',(154.938562860232,4.77853382687156,336.171242210241));
#42909=CARTESIAN_POINT('Ctrl Pts',(154.931151056055,4.80787859589356,336.044223913224));
#42910=CARTESIAN_POINT('Ctrl Pts',(154.923739251878,4.83211424495484,335.916436024065));
#42911=CARTESIAN_POINT('Ctrl Pts',(154.915964173099,4.85753775537083,335.782384869798));
#42912=CARTESIAN_POINT('Ctrl Pts',(154.908189094321,4.87741899903553,335.647063149466));
#42913=CARTESIAN_POINT('Ctrl Pts',(154.900414015543,4.89163509187614,335.510968874224));
#42914=CARTESIAN_POINT('Ctrl Pts',(154.892648504494,4.90583369090947,335.375042071653));
#42915=CARTESIAN_POINT('Ctrl Pts',(154.884882993445,4.91438096984336,335.238344990791));
#42916=CARTESIAN_POINT('Ctrl Pts',(154.877117482396,4.91720487979926,335.101386550283));
#42917=CARTESIAN_POINT('Ctrl Pts',(154.869359670873,4.92002598984022,334.964563904468));
#42918=CARTESIAN_POINT('Ctrl Pts',(154.861601859351,4.91713501594497,334.82748080298));
#42919=CARTESIAN_POINT('Ctrl Pts',(154.853844047829,4.90851165517153,334.690651663096));
#42920=CARTESIAN_POINT('Ctrl Pts',(154.846092074306,4.89989478375052,334.553925491478));
#42921=CARTESIAN_POINT('Ctrl Pts',(154.838340100783,4.88555413635134,334.41745328959));
#42922=CARTESIAN_POINT('Ctrl Pts',(154.83058812726,4.86552148057395,334.281749497339));
#42923=CARTESIAN_POINT('Ctrl Pts',(154.822839436702,4.84549730863821,334.146103175724));
#42924=CARTESIAN_POINT('Ctrl Pts',(154.815090746145,4.81978597973966,334.011225002383));
#42925=CARTESIAN_POINT('Ctrl Pts',(154.807342055587,4.7884710917699,333.877624097825));
#42926=CARTESIAN_POINT('Ctrl Pts',(154.799594977209,4.75716271912418,333.74405099005));
#42927=CARTESIAN_POINT('Ctrl Pts',(154.791847898831,4.72025319554371,333.611755002791));
#42928=CARTESIAN_POINT('Ctrl Pts',(154.784100820454,4.67787711945422,333.481234475705));
#42929=CARTESIAN_POINT('Ctrl Pts',(154.776353677148,4.63550068821224,333.350712854731));
#42930=CARTESIAN_POINT('Ctrl Pts',(154.768606533842,4.58765773378256,333.22196709538));
#42931=CARTESIAN_POINT('Ctrl Pts',(154.760859390536,4.53453243626125,333.09547941807));
#42932=CARTESIAN_POINT('Ctrl Pts',(154.753110505508,4.48139519504535,332.968963303646));
#42933=CARTESIAN_POINT('Ctrl Pts',(154.74536162048,4.4229733989114,332.844706641768));
#42934=CARTESIAN_POINT('Ctrl Pts',(154.737612735452,4.35949881853884,332.723170381065));
#42935=CARTESIAN_POINT('Ctrl Pts',(154.729855625677,4.29595686559076,332.60150512052));
#42936=CARTESIAN_POINT('Ctrl Pts',(154.722098515902,4.227351596389,332.482566376142));
#42937=CARTESIAN_POINT('Ctrl Pts',(154.714341406128,4.15396036129341,332.366789719885));
#42938=CARTESIAN_POINT('Ctrl Pts',(154.706580151201,4.08052990826851,332.250951196285));
#42939=CARTESIAN_POINT('Ctrl Pts',(154.698818896275,4.00230861616061,332.138278448644));
#42940=CARTESIAN_POINT('Ctrl Pts',(154.691057641349,3.9196158109255,332.029176047417));
#42941=CARTESIAN_POINT('Ctrl Pts',(154.683283970944,3.83679072415144,331.919899117904));
#42942=CARTESIAN_POINT('Ctrl Pts',(154.67551030054,3.74948007957757,331.814204249367));
#42943=CARTESIAN_POINT('Ctrl Pts',(154.667736630135,3.65804252361451,331.712461717648));
#42944=CARTESIAN_POINT('Ctrl Pts',(154.660324825958,3.57086140788074,331.61545532526));
#42945=CARTESIAN_POINT('Ctrl Pts',(154.652913021781,3.47992915042439,331.522041794123));
#42946=CARTESIAN_POINT('Ctrl Pts',(154.645501217604,3.38558488854456,331.432508160492));
#42947=CARTESIAN_POINT('Ctrl Pts',(154.637726138826,3.28661653335231,331.338586216769));
#42948=CARTESIAN_POINT('Ctrl Pts',(154.629951060047,3.18358049349499,331.248637307193));
#42949=CARTESIAN_POINT('Ctrl Pts',(154.622175981269,3.07682905755571,331.163034270015));
#42950=CARTESIAN_POINT('Ctrl Pts',(154.61441047022,2.97020898605451,331.077536572824));
#42951=CARTESIAN_POINT('Ctrl Pts',(154.606644959171,2.85988291752784,330.996374349489));
#42952=CARTESIAN_POINT('Ctrl Pts',(154.598879448122,2.74623982273755,330.919883592529));
#42953=CARTESIAN_POINT('Ctrl Pts',(154.591121636599,2.63270940540648,330.843468676378));
#42954=CARTESIAN_POINT('Ctrl Pts',(154.583363825077,2.51586882896713,330.771716225961));
#42955=CARTESIAN_POINT('Ctrl Pts',(154.575606013555,2.39613969079377,330.704921695161));
#42956=CARTESIAN_POINT('Ctrl Pts',(154.567854040032,2.27650065259376,330.638177429363));
#42957=CARTESIAN_POINT('Ctrl Pts',(154.560102066509,2.15397771934535,330.57638384649));
#42958=CARTESIAN_POINT('Ctrl Pts',(154.552350092986,2.02902068581284,330.519792625442));
#42959=CARTESIAN_POINT('Ctrl Pts',(154.544601402428,1.90411657165833,330.46322537081));
#42960=CARTESIAN_POINT('Ctrl Pts',(154.536852711871,1.77678076281382,330.411856256905));
#42961=CARTESIAN_POINT('Ctrl Pts',(154.529104021313,1.64748662919201,330.365890498798));
#42962=CARTESIAN_POINT('Ctrl Pts',(154.521356942935,1.51821939629449,330.31993430425));
#42963=CARTESIAN_POINT('Ctrl Pts',(154.513609864557,1.38699501711946,330.279379360211));
#42964=CARTESIAN_POINT('Ctrl Pts',(154.50586278618,1.2543053950483,330.244382160176));
#42965=CARTESIAN_POINT('Ctrl Pts',(154.498115642874,1.12161466091073,330.209384666831));
#42966=CARTESIAN_POINT('Ctrl Pts',(154.490368499568,0.987459037332595,330.17994511008));
#42967=CARTESIAN_POINT('Ctrl Pts',(154.482621356262,0.852343704169711,330.156169566091));
#42968=CARTESIAN_POINT('Ctrl Pts',(154.474872471234,0.717197994211744,330.132388676855));
#42969=CARTESIAN_POINT('Ctrl Pts',(154.467123586206,0.581092530209212,330.11427440201));
#42970=CARTESIAN_POINT('Ctrl Pts',(154.459374701178,0.444540358112609,330.101881286401));
#42971=CARTESIAN_POINT('Ctrl Pts',(154.451617591403,0.307843248129065,330.089475016611));
#42972=CARTESIAN_POINT('Ctrl Pts',(154.443860481629,0.17069887280036,330.082802071825));
#42973=CARTESIAN_POINT('Ctrl Pts',(154.436103371854,0.0336236040688946,
330.081864935186));
#42974=CARTESIAN_POINT('Ctrl Pts',(154.428342116928,-0.103524913303038,
330.080927297772));
#42975=CARTESIAN_POINT('Ctrl Pts',(154.420580862002,-0.240603860058357,
330.085731562174));
#42976=CARTESIAN_POINT('Ctrl Pts',(154.412819607075,-0.377100218672374,
330.096228136671));
#42977=CARTESIAN_POINT('Ctrl Pts',(154.405045936671,-0.513814926976299,
330.106741502267));
#42978=CARTESIAN_POINT('Ctrl Pts',(154.397272266266,-0.649944796492763,
330.122965327844));
#42979=CARTESIAN_POINT('Ctrl Pts',(154.389498595861,-0.784984370213917,
330.14479839749));
#42980=CARTESIAN_POINT('Ctrl Pts',(154.382086791684,-0.913737819290731,
330.165615132491));
#42981=CARTESIAN_POINT('Ctrl Pts',(154.374674987507,-1.04149991271711,330.191530585975));
#42982=CARTESIAN_POINT('Ctrl Pts',(154.36726318333,-1.16784574893145,330.22241490194));
#42983=CARTESIAN_POINT('Ctrl Pts',(154.359488104552,-1.30038417094281,330.25481295023));
#42984=CARTESIAN_POINT('Ctrl Pts',(154.351713025773,-1.4317828413548,330.292781638085));
#42985=CARTESIAN_POINT('Ctrl Pts',(154.343937946995,-1.56153758896135,330.33622648269));
#42986=CARTESIAN_POINT('Ctrl Pts',(154.336172435946,-1.69113266509016,330.379617865648));
#42987=CARTESIAN_POINT('Ctrl Pts',(154.328406924897,-1.81908747640063,330.428471874242));
#42988=CARTESIAN_POINT('Ctrl Pts',(154.320641413848,-1.94490898521745,330.482643239491));
#42989=CARTESIAN_POINT('Ctrl Pts',(154.312883602326,-2.0706057416418,330.536760893673));
#42990=CARTESIAN_POINT('Ctrl Pts',(154.305125790803,-2.19417304819069,330.596185259009));
#42991=CARTESIAN_POINT('Ctrl Pts',(154.297367979281,-2.3151343008612,330.660721692323));
#42992=CARTESIAN_POINT('Ctrl Pts',(154.289616005758,-2.4360045263529,330.725209559924));
#42993=CARTESIAN_POINT('Ctrl Pts',(154.281864032235,-2.55427225804356,330.794801654997));
#42994=CARTESIAN_POINT('Ctrl Pts',(154.274112058712,-2.66948244402078,330.869255933423));
#42995=CARTESIAN_POINT('Ctrl Pts',(154.266363368155,-2.78464383841632,330.943678680418));
#42996=CARTESIAN_POINT('Ctrl Pts',(154.258614677597,-2.89674993490381,331.022959303572));
#42997=CARTESIAN_POINT('Ctrl Pts',(154.250865987039,-3.00537199613136,331.106810789678));
#42998=CARTESIAN_POINT('Ctrl Pts',(154.243118908662,-3.1139714576321,331.190644829781));
#42999=CARTESIAN_POINT('Ctrl Pts',(154.235371830284,-3.21908801650164,331.279047602517));
#43000=CARTESIAN_POINT('Ctrl Pts',(154.227624751906,-3.32032387687554,331.371690143448));
#43001=CARTESIAN_POINT('Ctrl Pts',(154.2198776086,-3.42156058570353,331.464333460813));
#43002=CARTESIAN_POINT('Ctrl Pts',(154.212130465294,-3.51891624280707,331.561216353366));
#43003=CARTESIAN_POINT('Ctrl Pts',(154.204383321988,-3.61202826466784,331.66197140849));
#43004=CARTESIAN_POINT('Ctrl Pts',(154.19663443696,-3.70516122008752,331.762749115488));
#43005=CARTESIAN_POINT('Ctrl Pts',(154.188885551932,-3.79404837655751,331.867400430336));
#43006=CARTESIAN_POINT('Ctrl Pts',(154.181136666904,-3.87836622755252,331.975523439092));
#43007=CARTESIAN_POINT('Ctrl Pts',(154.173379557129,-3.96277357438588,332.083761210728));
#43008=CARTESIAN_POINT('Ctrl Pts',(154.165622447355,-4.04260168685022,332.195477728472));
#43009=CARTESIAN_POINT('Ctrl Pts',(154.15786533758,-4.11756903833055,332.310240107913));
#43010=CARTESIAN_POINT('Ctrl Pts',(154.150104082654,-4.19257644996644,332.4250638127));
#43011=CARTESIAN_POINT('Ctrl Pts',(154.142342827728,-4.26271772521411,332.542936286614));
#43012=CARTESIAN_POINT('Ctrl Pts',(154.134581572801,-4.32775694359023,332.663399285349));
#43013=CARTESIAN_POINT('Ctrl Pts',(154.126807902397,-4.39290020351956,332.784054985623));
#43014=CARTESIAN_POINT('Ctrl Pts',(154.119034231992,-4.45292492599718,332.907309140046));
#43015=CARTESIAN_POINT('Ctrl Pts',(154.111260561587,-4.5076426938536,333.032681925298));
#43016=CARTESIAN_POINT('Ctrl Pts',(154.10384875741,-4.55981333645127,333.152218577232));
#43017=CARTESIAN_POINT('Ctrl Pts',(154.096436953233,-4.60715987847357,333.273680786186));
#43018=CARTESIAN_POINT('Ctrl Pts',(154.089025149056,-4.64956157998799,333.396640970837));
#43019=CARTESIAN_POINT('Ctrl Pts',(154.079880925922,-4.70187416281465,333.548341601099));
#43020=CARTESIAN_POINT('Ctrl Pts',(154.070736702789,-4.74679633555163,333.702713734351));
#43021=CARTESIAN_POINT('Ctrl Pts',(154.061592479655,-4.78408881765321,333.859089290389));
#43022=CARTESIAN_POINT('Ctrl Pts',(154.052490952621,-4.82120717413257,334.014734699505));
#43023=CARTESIAN_POINT('Ctrl Pts',(154.043389425587,-4.85076683947267,334.172364783848));
#43024=CARTESIAN_POINT('Ctrl Pts',(154.034287898553,-4.87257861659285,334.331299254059));
#43025=CARTESIAN_POINT('Ctrl Pts',(154.025265126919,-4.89420165667757,334.488858466281));
#43026=CARTESIAN_POINT('Ctrl Pts',(154.016242355285,-4.90821023847201,334.647699488882));
#43027=CARTESIAN_POINT('Ctrl Pts',(154.007219583651,-4.91446721116948,334.807139706419));
#43028=CARTESIAN_POINT('Ctrl Pts',(154.003658471948,-4.91693671606248,334.870067645598));
#43029=CARTESIAN_POINT('Ctrl Pts',(154.000097360245,-4.91819925871801,334.933088712353));
#43030=CARTESIAN_POINT('Ctrl Pts',(153.996536248542,-4.91824850103284,334.996160131745));
#43031=CARTESIAN_POINT('',(157.496536248451,-4.91824791444093,335.004529304303));
#43032=CARTESIAN_POINT('Ctrl Pts',(157.496536248451,-4.91824791444093,335.004529304303));
#43033=CARTESIAN_POINT('Ctrl Pts',(157.486533103091,-4.91808521296232,335.181202398966));
#43034=CARTESIAN_POINT('Ctrl Pts',(157.476529957731,-4.90839940609836,335.357450971929));
#43035=CARTESIAN_POINT('Ctrl Pts',(157.466526812371,-4.88934810921038,335.532407860067));
#43036=CARTESIAN_POINT('Ctrl Pts',(157.456290198198,-4.86985216381327,335.711448161524));
#43037=CARTESIAN_POINT('Ctrl Pts',(157.446053584026,-4.84054843538798,335.889136075352));
#43038=CARTESIAN_POINT('Ctrl Pts',(157.435816969853,-4.80165374290327,336.064567703701));
#43039=CARTESIAN_POINT('Ctrl Pts',(157.43317183335,-4.79160337183968,336.109899157649));
#43040=CARTESIAN_POINT('Ctrl Pts',(157.430526696846,-4.78091285455322,336.155080074558));
#43041=CARTESIAN_POINT('Ctrl Pts',(157.427881560343,-4.76958644365158,336.200095087497));
#43042=CARTESIAN_POINT('Ctrl Pts',(157.420106481565,-4.73629374328191,336.332411613088));
#43043=CARTESIAN_POINT('Ctrl Pts',(157.412331402786,-4.69743823030342,336.463550779452));
#43044=CARTESIAN_POINT('Ctrl Pts',(157.404556324008,-4.6531177914097,336.593009065187));
#43045=CARTESIAN_POINT('Ctrl Pts',(157.396790812959,-4.60885189163762,336.722308044259));
#43046=CARTESIAN_POINT('Ctrl Pts',(157.38902530191,-4.55913457204411,336.849929892019));
#43047=CARTESIAN_POINT('Ctrl Pts',(157.381259790861,-4.5041144291156,336.975382563437));
#43048=CARTESIAN_POINT('Ctrl Pts',(157.373501979338,-4.44914883881894,337.100710848167));
#43049=CARTESIAN_POINT('Ctrl Pts',(157.365744167816,-4.38889104441723,337.223873881003));
#43050=CARTESIAN_POINT('Ctrl Pts',(157.357986356294,-4.32353890444586,337.344396383772));
#43051=CARTESIAN_POINT('Ctrl Pts',(157.350234382771,-4.25823594403232,337.464828189536));
#43052=CARTESIAN_POINT('Ctrl Pts',(157.342482409248,-4.18784645432413,337.582623078197));
#43053=CARTESIAN_POINT('Ctrl Pts',(157.334730435725,-4.1126155481167,337.697327643407));
#43054=CARTESIAN_POINT('Ctrl Pts',(157.326981745167,-4.0374165022427,337.811983631166));
#43055=CARTESIAN_POINT('Ctrl Pts',(157.31923305461,-3.95738033177873,337.923551572327));
#43056=CARTESIAN_POINT('Ctrl Pts',(157.311484364052,-3.87279693981029,338.031604678301));
#43057=CARTESIAN_POINT('Ctrl Pts',(157.303737285674,-3.78823114612297,338.139635302923));
#43058=CARTESIAN_POINT('Ctrl Pts',(157.295990207296,-3.69912025354925,338.244152239353));
#43059=CARTESIAN_POINT('Ctrl Pts',(157.288243128919,-3.60579590641386,338.344759923192));
#43060=CARTESIAN_POINT('Ctrl Pts',(157.280495985613,-3.5124707771306,338.44536845022));
#43061=CARTESIAN_POINT('Ctrl Pts',(157.272748842307,-3.41493238867397,338.542067372741));
#43062=CARTESIAN_POINT('Ctrl Pts',(157.265001699001,-3.31355059478758,338.634496597644));
#43063=CARTESIAN_POINT('Ctrl Pts',(157.257252813973,-3.21214600812157,338.726946602599));
#43064=CARTESIAN_POINT('Ctrl Pts',(157.249503928945,-3.10689658539734,338.815124736515));
#43065=CARTESIAN_POINT('Ctrl Pts',(157.241755043917,-2.99820641690037,338.898710215463));
#43066=CARTESIAN_POINT('Ctrl Pts',(157.233997934142,-2.88940088353549,338.982384412903));
#43067=CARTESIAN_POINT('Ctrl Pts',(157.226240824367,-2.77714761943565,339.061455979065));
#43068=CARTESIAN_POINT('Ctrl Pts',(157.218483714593,-2.66188140104686,339.135646318202));
#43069=CARTESIAN_POINT('Ctrl Pts',(157.210722459666,-2.54655358807648,339.209876302284));
#43070=CARTESIAN_POINT('Ctrl Pts',(157.20296120474,-2.42820994976775,339.279219664418));
#43071=CARTESIAN_POINT('Ctrl Pts',(157.195199949814,-2.30731031378142,339.343443585269));
#43072=CARTESIAN_POINT('Ctrl Pts',(157.187426279409,-2.18621727777866,339.407770243464));
#43073=CARTESIAN_POINT('Ctrl Pts',(157.179652609005,-2.06256042628889,339.466960926604));
#43074=CARTESIAN_POINT('Ctrl Pts',(157.1718789386,-1.93682084457429,339.520830463369));
#43075=CARTESIAN_POINT('Ctrl Pts',(157.164467134423,-1.81693447064047,339.572192360236));
#43076=CARTESIAN_POINT('Ctrl Pts',(157.157055330246,-1.69515517386244,339.618717258106));
#43077=CARTESIAN_POINT('Ctrl Pts',(157.149643526069,-1.57191134148936,339.660287308417));
#43078=CARTESIAN_POINT('Ctrl Pts',(157.141868447291,-1.44262696176637,339.703894830726));
#43079=CARTESIAN_POINT('Ctrl Pts',(157.134093368512,-1.31132229143814,339.742187328599));
#43080=CARTESIAN_POINT('Ctrl Pts',(157.126318289734,-1.17847372450055,339.774974632724));
#43081=CARTESIAN_POINT('Ctrl Pts',(157.118552778685,-1.04578863618212,339.807721589985));
#43082=CARTESIAN_POINT('Ctrl Pts',(157.110787267636,-0.91156380729692,339.834976740029));
#43083=CARTESIAN_POINT('Ctrl Pts',(157.103021756587,-0.776293423092196,
339.856598767014));
#43084=CARTESIAN_POINT('Ctrl Pts',(157.095263945064,-0.641157159867239,
339.878199355697));
#43085=CARTESIAN_POINT('Ctrl Pts',(157.087506133542,-0.504977787845208,
339.894177875002));
#43086=CARTESIAN_POINT('Ctrl Pts',(157.07974832202,-0.368262051188472,339.904443508101));
#43087=CARTESIAN_POINT('Ctrl Pts',(157.071996348497,-0.23164919745919,339.914701415986));
#43088=CARTESIAN_POINT('Ctrl Pts',(157.064244374974,-0.0945011707113606,
339.91925496572));
#43089=CARTESIAN_POINT('Ctrl Pts',(157.056492401451,0.0426681053860614,
339.918064913691));
#43090=CARTESIAN_POINT('Ctrl Pts',(157.048743710893,0.179779290213689,339.91687536565));
#43091=CARTESIAN_POINT('Ctrl Pts',(157.040995020336,0.316911316446174,339.90994705714));
#43092=CARTESIAN_POINT('Ctrl Pts',(157.033246329778,0.453548405259294,339.897292814054));
#43093=CARTESIAN_POINT('Ctrl Pts',(157.0254992514,0.590157065584847,339.88464120379));
#43094=CARTESIAN_POINT('Ctrl Pts',(157.017752173023,0.726270604352937,339.866266064609));
#43095=CARTESIAN_POINT('Ctrl Pts',(157.010005094645,0.861376911248659,339.842232220709));
#43096=CARTESIAN_POINT('Ctrl Pts',(157.002257951339,0.996484350465272,339.818198175381));
#43097=CARTESIAN_POINT('Ctrl Pts',(156.994510808033,1.13058415613934,339.788505399197));
#43098=CARTESIAN_POINT('Ctrl Pts',(156.986763664727,1.26317336920926,339.753270043015));
#43099=CARTESIAN_POINT('Ctrl Pts',(156.979014779699,1.39579239114918,339.718026765177));
#43100=CARTESIAN_POINT('Ctrl Pts',(156.971265894671,1.52689976700366,339.677238528132));
#43101=CARTESIAN_POINT('Ctrl Pts',(156.963517009643,1.65600706628379,339.631071545433));
#43102=CARTESIAN_POINT('Ctrl Pts',(156.955759899868,1.78525140138543,339.584855560621));
#43103=CARTESIAN_POINT('Ctrl Pts',(156.948002790094,1.91249105058461,339.533249557597));
#43104=CARTESIAN_POINT('Ctrl Pts',(156.940245680319,2.03725645429074,339.476468385005));
#43105=CARTESIAN_POINT('Ctrl Pts',(156.932484425393,2.16208852863936,339.41965687037));
#43106=CARTESIAN_POINT('Ctrl Pts',(156.924723170467,2.28444337447842,339.357664852337));
#43107=CARTESIAN_POINT('Ctrl Pts',(156.91696191554,2.40387636993161,339.290753017896));
#43108=CARTESIAN_POINT('Ctrl Pts',(156.909188245136,2.5235004192544,339.223734146327));
#43109=CARTESIAN_POINT('Ctrl Pts',(156.901414574731,2.64019294525471,339.151779936814));
#43110=CARTESIAN_POINT('Ctrl Pts',(156.893640904326,2.75353789057768,339.07519473739));
#43111=CARTESIAN_POINT('Ctrl Pts',(156.886229100149,2.86160660142614,339.002174597426));
#43112=CARTESIAN_POINT('Ctrl Pts',(156.878817295972,2.96663214579147,338.924945080553));
#43113=CARTESIAN_POINT('Ctrl Pts',(156.871405491795,3.0682835973832,338.843802652131));
#43114=CARTESIAN_POINT('Ctrl Pts',(156.863630413017,3.1749172894221,338.758683191581));
#43115=CARTESIAN_POINT('Ctrl Pts',(156.855855334238,3.27817475919368,338.668988560862));
#43116=CARTESIAN_POINT('Ctrl Pts',(156.84808025546,3.37763828513822,338.575016458321));
#43117=CARTESIAN_POINT('Ctrl Pts',(156.840314744411,3.47697941488193,338.481159994436));
#43118=CARTESIAN_POINT('Ctrl Pts',(156.832549233362,3.57253560874617,338.383036797854));
#43119=CARTESIAN_POINT('Ctrl Pts',(156.824783722313,3.66392059923009,338.280985965383));
#43120=CARTESIAN_POINT('Ctrl Pts',(156.817025910791,3.75521498122989,338.179036316609));
#43121=CARTESIAN_POINT('Ctrl Pts',(156.809268099269,3.84234613117196,338.073167071059));
#43122=CARTESIAN_POINT('Ctrl Pts',(156.801510287746,3.92496345090526,337.963755214514));
#43123=CARTESIAN_POINT('Ctrl Pts',(156.793758314223,4.00751859848546,337.854425693861));
#43124=CARTESIAN_POINT('Ctrl Pts',(156.7860063407,4.08556644242812,337.741559179287));
#43125=CARTESIAN_POINT('Ctrl Pts',(156.778254367177,4.15879586835624,337.625566603201));
#43126=CARTESIAN_POINT('Ctrl Pts',(156.77050567662,4.23199428157903,337.509623150039));
#43127=CARTESIAN_POINT('Ctrl Pts',(156.762756986062,4.30037812717194,337.390556598315));
#43128=CARTESIAN_POINT('Ctrl Pts',(156.755008295505,4.36367907318612,337.268807618274));
#43129=CARTESIAN_POINT('Ctrl Pts',(156.747261217127,4.42696684890979,337.147083969125));
#43130=CARTESIAN_POINT('Ctrl Pts',(156.739514138749,4.48517364837742,337.022679348344));
#43131=CARTESIAN_POINT('Ctrl Pts',(156.731767060371,4.53807685136121,336.896059480512));
#43132=CARTESIAN_POINT('Ctrl Pts',(156.724019917065,4.59098049772476,336.769438551484));
#43133=CARTESIAN_POINT('Ctrl Pts',(156.71627277376,4.6385803082592,336.640602699034));
#43134=CARTESIAN_POINT('Ctrl Pts',(156.708525630454,4.68070177669209,336.510037728062));
#43135=CARTESIAN_POINT('Ctrl Pts',(156.700776745426,4.72283271492532,336.379443403313));
#43136=CARTESIAN_POINT('Ctrl Pts',(156.693027860398,4.75948274023017,336.247119558411));
#43137=CARTESIAN_POINT('Ctrl Pts',(156.685278975369,4.79052730736479,336.113566872663));
#43138=CARTESIAN_POINT('Ctrl Pts',(156.677521865595,4.82160482552374,335.979872432715));
#43139=CARTESIAN_POINT('Ctrl Pts',(156.66976475582,4.84706491180638,335.844946927776));
#43140=CARTESIAN_POINT('Ctrl Pts',(156.662007646045,4.86683413138314,335.709301487454));
#43141=CARTESIAN_POINT('Ctrl Pts',(156.654246391119,4.88661391499873,335.573583562545));
#43142=CARTESIAN_POINT('Ctrl Pts',(156.646485136193,4.90069673229623,335.437145324294));
#43143=CARTESIAN_POINT('Ctrl Pts',(156.638723881267,4.90906119011706,335.30050173741));
#43144=CARTESIAN_POINT('Ctrl Pts',(156.630950210862,4.91743902834443,335.163639565319));
#43145=CARTESIAN_POINT('Ctrl Pts',(156.623176540458,4.92008022012367,335.02657177918));
#43146=CARTESIAN_POINT('Ctrl Pts',(156.615402870053,4.91701554570077,334.889812950684));
#43147=CARTESIAN_POINT('Ctrl Pts',(156.607991065876,4.91409353260957,334.759420278556));
#43148=CARTESIAN_POINT('Ctrl Pts',(156.600579261699,4.90598493267237,334.629308734669));
#43149=CARTESIAN_POINT('Ctrl Pts',(156.593167457522,4.89275996672966,334.499917036415));
#43150=CARTESIAN_POINT('Ctrl Pts',(156.585392378743,4.87888680581097,334.364183465593));
#43151=CARTESIAN_POINT('Ctrl Pts',(156.577617299965,4.85933921909417,334.228813145002));
#43152=CARTESIAN_POINT('Ctrl Pts',(156.569842221186,4.83414149436549,334.094318447271));
#43153=CARTESIAN_POINT('Ctrl Pts',(156.562076710137,4.80897477704125,333.959989253828));
#43154=CARTESIAN_POINT('Ctrl Pts',(156.554311199088,4.77817182718233,333.826533919828));
#43155=CARTESIAN_POINT('Ctrl Pts',(156.546545688039,4.74180876701852,333.694460770591));
#43156=CARTESIAN_POINT('Ctrl Pts',(156.538787876517,4.70548176093474,333.562518572266));
#43157=CARTESIAN_POINT('Ctrl Pts',(156.531030064995,4.66360571854861,333.431956205875));
#43158=CARTESIAN_POINT('Ctrl Pts',(156.523272253473,4.61630792646881,333.303272505521));
#43159=CARTESIAN_POINT('Ctrl Pts',(156.51552027995,4.56904572747745,333.174685643732));
#43160=CARTESIAN_POINT('Ctrl Pts',(156.507768306427,4.51637003421296,333.047974999368));
#43161=CARTESIAN_POINT('Ctrl Pts',(156.500016332904,4.458458046662,332.923624574251));
#43162=CARTESIAN_POINT('Ctrl Pts',(156.492267642346,4.40057058487215,332.799326811613));
#43163=CARTESIAN_POINT('Ctrl Pts',(156.484518951788,4.33745140406873,332.677387633773));
#43164=CARTESIAN_POINT('Ctrl Pts',(156.476770261231,4.26932586344716,332.558271158748));
#43165=CARTESIAN_POINT('Ctrl Pts',(156.469023182853,4.20121449691332,332.439179466901));
#43166=CARTESIAN_POINT('Ctrl Pts',(156.461276104475,4.12809903633994,332.322909648801));
#43167=CARTESIAN_POINT('Ctrl Pts',(156.453529026097,4.05025064688352,332.209900940841));
#43168=CARTESIAN_POINT('Ctrl Pts',(156.445781882791,3.97240160498266,332.09689128576));
#43169=CARTESIAN_POINT('Ctrl Pts',(156.438034739485,3.88981977682201,331.987143117224));
#43170=CARTESIAN_POINT('Ctrl Pts',(156.43028759618,3.80281925074881,331.881066078187));
#43171=CARTESIAN_POINT('Ctrl Pts',(156.422538711152,3.71579916511037,331.77496519078));
#43172=CARTESIAN_POINT('Ctrl Pts',(156.414789826123,3.62435865259686,331.67253737739));
#43173=CARTESIAN_POINT('Ctrl Pts',(156.407040941095,3.52885134654363,331.57415831707));
#43174=CARTESIAN_POINT('Ctrl Pts',(156.399283831321,3.43324266804885,331.4756748362));
#43175=CARTESIAN_POINT('Ctrl Pts',(156.391526721546,3.33355884602364,331.381248973731));
#43176=CARTESIAN_POINT('Ctrl Pts',(156.383769611771,3.23018996045864,331.291219084139));
#43177=CARTESIAN_POINT('Ctrl Pts',(156.376008356845,3.12676583786634,331.201141085453));
#43178=CARTESIAN_POINT('Ctrl Pts',(156.368247101919,3.01965303305044,331.115463984402));
#43179=CARTESIAN_POINT('Ctrl Pts',(156.360485846993,2.90927301375598,331.034484447902));
#43180=CARTESIAN_POINT('Ctrl Pts',(156.352712176588,2.79871642240342,330.953375370535));
#43181=CARTESIAN_POINT('Ctrl Pts',(156.344938506183,2.68488249724977,330.876979091993));
#43182=CARTESIAN_POINT('Ctrl Pts',(156.337164835779,2.56822060956445,330.805548192778));
#43183=CARTESIAN_POINT('Ctrl Pts',(156.329753031601,2.4569893608182,330.737442419107));
#43184=CARTESIAN_POINT('Ctrl Pts',(156.322341227424,2.34318775905778,330.673850291587));
#43185=CARTESIAN_POINT('Ctrl Pts',(156.314929423247,2.2272227316258,330.614950175171));
#43186=CARTESIAN_POINT('Ctrl Pts',(156.307154344469,2.10557391275734,330.553163188596));
#43187=CARTESIAN_POINT('Ctrl Pts',(156.29937926569,1.98115980136051,330.496344523276));
#43188=CARTESIAN_POINT('Ctrl Pts',(156.291604186912,1.85442440602456,330.444751029324));
#43189=CARTESIAN_POINT('Ctrl Pts',(156.283838675863,1.72784496666089,330.393221024451));
#43190=CARTESIAN_POINT('Ctrl Pts',(156.276073164814,1.59895028551374,330.346903543247));
#43191=CARTESIAN_POINT('Ctrl Pts',(156.268307653765,1.46820901829683,330.306009656903));
#43192=CARTESIAN_POINT('Ctrl Pts',(156.260549842243,1.337597381427,330.265156316966));
#43193=CARTESIAN_POINT('Ctrl Pts',(156.252792030721,1.20514317272121,330.229715986273));
#43194=CARTESIAN_POINT('Ctrl Pts',(156.245034219198,1.07133475450583,330.199851574556));
#43195=CARTESIAN_POINT('Ctrl Pts',(156.237282245675,0.937627031368573,330.170009636757));
#43196=CARTESIAN_POINT('Ctrl Pts',(156.229530272153,0.802567507113986,330.145735350689));
#43197=CARTESIAN_POINT('Ctrl Pts',(156.22177829863,0.666659082280117,330.127141626262));
#43198=CARTESIAN_POINT('Ctrl Pts',(156.214029608072,0.530808214744785,330.108555776288));
#43199=CARTESIAN_POINT('Ctrl Pts',(156.206280917514,0.394109548130885,330.095645756016));
#43200=CARTESIAN_POINT('Ctrl Pts',(156.198532226957,0.257075323970763,330.088473216982));
#43201=CARTESIAN_POINT('Ctrl Pts',(156.190785148579,0.120069610925533,330.081302170254));
#43202=CARTESIAN_POINT('Ctrl Pts',(156.183038070201,-0.0172711307029542,
330.079866250765));
#43203=CARTESIAN_POINT('Ctrl Pts',(156.175290991823,-0.154430794635645,
330.084175125966));
#43204=CARTESIAN_POINT('Ctrl Pts',(156.167543848517,-0.291591608098359,
330.08848403728));
#43205=CARTESIAN_POINT('Ctrl Pts',(156.159796705212,-0.428570950156742,
330.098537827043));
#43206=CARTESIAN_POINT('Ctrl Pts',(156.152049561906,-0.564854372084219,
330.114294052971));
#43207=CARTESIAN_POINT('Ctrl Pts',(156.144300676878,-0.701168433418233,
330.130053821233));
#43208=CARTESIAN_POINT('Ctrl Pts',(156.13655179185,-0.836785875076158,330.151518531871));
#43209=CARTESIAN_POINT('Ctrl Pts',(156.128802906822,-0.971199409237683,
330.178594108562));
#43210=CARTESIAN_POINT('Ctrl Pts',(156.121045797047,-1.10575561131321,330.205698423549));
#43211=CARTESIAN_POINT('Ctrl Pts',(156.113288687272,-1.23910496950445,330.238425423815));
#43212=CARTESIAN_POINT('Ctrl Pts',(156.105531577498,-1.37075185965037,330.276630185793));
#43213=CARTESIAN_POINT('Ctrl Pts',(156.097770322571,-1.50246909768508,330.314855363174));
#43214=CARTESIAN_POINT('Ctrl Pts',(156.090009067645,-1.63248168461715,330.358564010365));
#43215=CARTESIAN_POINT('Ctrl Pts',(156.082247812719,-1.76031206652673,330.407562249639));
#43216=CARTESIAN_POINT('Ctrl Pts',(156.074474142314,-1.88834693538757,330.456638870128));
#43217=CARTESIAN_POINT('Ctrl Pts',(156.06670047191,-2.01419226454658,330.511021836393));
#43218=CARTESIAN_POINT('Ctrl Pts',(156.058926801505,-2.13739247309216,330.57046994835));
#43219=CARTESIAN_POINT('Ctrl Pts',(156.051514997328,-2.25485768229059,330.627150736394));
#43220=CARTESIAN_POINT('Ctrl Pts',(156.044103193151,-2.36991823564859,330.688435582049));
#43221=CARTESIAN_POINT('Ctrl Pts',(156.036691388974,-2.48220393053748,330.754078814942));
#43222=CARTESIAN_POINT('Ctrl Pts',(156.028916310195,-2.59999308181405,330.82293941822));
#43223=CARTESIAN_POINT('Ctrl Pts',(156.021141231417,-2.7151007242116,330.896814058694));
#43224=CARTESIAN_POINT('Ctrl Pts',(156.013366152639,-2.82707058846668,330.975468356401));
#43225=CARTESIAN_POINT('Ctrl Pts',(156.00560064159,-2.93890266667534,331.054025864988));
#43226=CARTESIAN_POINT('Ctrl Pts',(155.99783513054,-3.04760433270449,331.137351105436));
#43227=CARTESIAN_POINT('Ctrl Pts',(155.990069619491,-3.15274447578762,331.22516419789));
#43228=CARTESIAN_POINT('Ctrl Pts',(155.982311807969,-3.25778037211277,331.312890223407));
#43229=CARTESIAN_POINT('Ctrl Pts',(155.974553996447,-3.35926147482994,331.405094996791));
#43230=CARTESIAN_POINT('Ctrl Pts',(155.966796184925,-3.45678650879377,331.501456003546));
#43231=CARTESIAN_POINT('Ctrl Pts',(155.959044211402,-3.55423815207675,331.597744495588));
#43232=CARTESIAN_POINT('Ctrl Pts',(155.951292237879,-3.64773937538844,331.698182721853));
#43233=CARTESIAN_POINT('Ctrl Pts',(155.943540264356,-3.73692308204036,331.80240888458));
#43234=CARTESIAN_POINT('Ctrl Pts',(155.935791573798,-3.82606901933971,331.906590907465));
#43235=CARTESIAN_POINT('Ctrl Pts',(155.928042883241,-3.9109008230817,332.014557379813));
#43236=CARTESIAN_POINT('Ctrl Pts',(155.920294192683,-3.99108944589062,332.125910909975));
#43237=CARTESIAN_POINT('Ctrl Pts',(155.912547114305,-4.07126138478685,332.237241272105));
#43238=CARTESIAN_POINT('Ctrl Pts',(155.904800035927,-4.14679183602421,332.351956973348));
#43239=CARTESIAN_POINT('Ctrl Pts',(155.897052957549,-4.21739337531564,332.469629240537));
#43240=CARTESIAN_POINT('Ctrl Pts',(155.889305814244,-4.28799550631593,332.587302493933));
#43241=CARTESIAN_POINT('Ctrl Pts',(155.881558670938,-4.35366844187699,332.707932027524));
#43242=CARTESIAN_POINT('Ctrl Pts',(155.873811527632,-4.41416947489604,332.831062262444));
#43243=CARTESIAN_POINT('Ctrl Pts',(155.866062642604,-4.47468410983167,332.954220179654));
#43244=CARTESIAN_POINT('Ctrl Pts',(155.858313757576,-4.53002435613471,333.079879566187));
#43245=CARTESIAN_POINT('Ctrl Pts',(155.850564872548,-4.57999480204501,333.207562922795));
#43246=CARTESIAN_POINT('Ctrl Pts',(155.842807762773,-4.63001828710295,333.335381803836));
#43247=CARTESIAN_POINT('Ctrl Pts',(155.835050652998,-4.67466044368149,333.465228581742));
#43248=CARTESIAN_POINT('Ctrl Pts',(155.827293543223,-4.71377493042639,333.596608049124));
#43249=CARTESIAN_POINT('Ctrl Pts',(155.819532288297,-4.75291031870232,333.728057721493));
#43250=CARTESIAN_POINT('Ctrl Pts',(155.811771033371,-4.78651205570566,333.861041336538));
#43251=CARTESIAN_POINT('Ctrl Pts',(155.804009778445,-4.81448474552528,333.995052390617));
#43252=CARTESIAN_POINT('Ctrl Pts',(155.79623610804,-4.84250218253236,334.129277818709));
#43253=CARTESIAN_POINT('Ctrl Pts',(155.788462437635,-4.86487251460147,334.264533584332));
#43254=CARTESIAN_POINT('Ctrl Pts',(155.78068876723,-4.88155203105705,334.400306052571));
#43255=CARTESIAN_POINT('Ctrl Pts',(155.773276963053,-4.89745511200852,334.529758279747));
#43256=CARTESIAN_POINT('Ctrl Pts',(155.765865158876,-4.90818524543721,334.65967990028));
#43257=CARTESIAN_POINT('Ctrl Pts',(155.758453354699,-4.91374868291656,334.789626656546));
#43258=CARTESIAN_POINT('Ctrl Pts',(155.754480985963,-4.91673041645718,334.859271836005));
#43259=CARTESIAN_POINT('Ctrl Pts',(155.750508617226,-4.91823155793977,334.928980857133));
#43260=CARTESIAN_POINT('Ctrl Pts',(155.74653624849,-4.9182498311247,334.998711147067));
#43261=CARTESIAN_POINT('',(159.246536248535,-4.91824990229953,334.999019678274));
#43262=CARTESIAN_POINT('Ctrl Pts',(159.24653624849,-4.91824990229969,334.999019679075));
#43263=CARTESIAN_POINT('Ctrl Pts',(159.238532934143,-4.91827822418977,335.14111001863));
#43264=CARTESIAN_POINT('Ctrl Pts',(159.230529619796,-4.91214462811284,335.283122174808));
#43265=CARTESIAN_POINT('Ctrl Pts',(159.222526305449,-4.89989552381521,335.424507854104));
#43266=CARTESIAN_POINT('Ctrl Pts',(159.214516214359,-4.88763604768447,335.566013250615));
#43267=CARTESIAN_POINT('Ctrl Pts',(159.206506123268,-4.86925076832775,335.7068907614));
#43268=CARTESIAN_POINT('Ctrl Pts',(159.198496032178,-4.84483770014801,335.846599504916));
#43269=CARTESIAN_POINT('Ctrl Pts',(159.190063843328,-4.8191381670273,335.993670305474));
#43270=CARTESIAN_POINT('Ctrl Pts',(159.181631654479,-4.7867584610174,336.139445373955));
#43271=CARTESIAN_POINT('Ctrl Pts',(159.17319946563,-4.74787291413732,336.283310505568));
#43272=CARTESIAN_POINT('Ctrl Pts',(159.165166204723,-4.71082704749778,336.42036935924));
#43273=CARTESIAN_POINT('Ctrl Pts',(159.157132943816,-4.66787693508807,336.555694534693));
#43274=CARTESIAN_POINT('Ctrl Pts',(159.149099682909,-4.61922322496871,336.688774662413));
#43275=CARTESIAN_POINT('Ctrl Pts',(159.141057776062,-4.57051715042545,336.821998019996));
#43276=CARTESIAN_POINT('Ctrl Pts',(159.133015869215,-4.51609536852315,336.952971185732));
#43277=CARTESIAN_POINT('Ctrl Pts',(159.124973962368,-4.45620553497504,337.081205249983));
#43278=CARTESIAN_POINT('Ctrl Pts',(159.116917656263,-4.39620846701454,337.209668920892));
#43279=CARTESIAN_POINT('Ctrl Pts',(159.108861350158,-4.33072395016572,337.335383380747));
#43280=CARTESIAN_POINT('Ctrl Pts',(159.100805044053,-4.26004465514347,337.457885798544));
#43281=CARTESIAN_POINT('Ctrl Pts',(159.099639951364,-4.24982310586148,337.475601941585));
#43282=CARTESIAN_POINT('Ctrl Pts',(159.098474858675,-4.23949298126891,337.493250959373));
#43283=CARTESIAN_POINT('Ctrl Pts',(159.097309765986,-4.22905523794468,337.510831507073));
#43284=CARTESIAN_POINT('Ctrl Pts',(159.089534687208,-4.15940045649074,337.628152767989));
#43285=CARTESIAN_POINT('Ctrl Pts',(159.08175960843,-4.08474986776342,337.742758707826));
#43286=CARTESIAN_POINT('Ctrl Pts',(159.073984529651,-4.00534092879957,337.854194651138));
#43287=CARTESIAN_POINT('Ctrl Pts',(159.066219018602,-3.92602970759045,337.965493465427));
#43288=CARTESIAN_POINT('Ctrl Pts',(159.058453507553,-3.84197201148367,338.073629729549));
#43289=CARTESIAN_POINT('Ctrl Pts',(159.050687996504,-3.75345062640725,338.178174233365));
#43290=CARTESIAN_POINT('Ctrl Pts',(159.042930184982,-3.66501701054178,338.282615081));
#43291=CARTESIAN_POINT('Ctrl Pts',(159.03517237346,-3.57212876417649,338.383470959018));
#43292=CARTESIAN_POINT('Ctrl Pts',(159.027414561938,-3.47511110534665,338.480342780244));
#43293=CARTESIAN_POINT('Ctrl Pts',(159.019662588415,-3.37816645538184,338.577141702353));
#43294=CARTESIAN_POINT('Ctrl Pts',(159.011910614892,-3.27709885379081,338.66996226023));
#43295=CARTESIAN_POINT('Ctrl Pts',(159.004158641369,-3.1722725700779,338.758439809766));
#43296=CARTESIAN_POINT('Ctrl Pts',(158.996409950811,-3.06749068035845,338.846879889007));
#43297=CARTESIAN_POINT('Ctrl Pts',(158.988661260253,-2.95895357258093,338.930980366488));
#43298=CARTESIAN_POINT('Ctrl Pts',(158.980912569696,-2.84706085227632,339.010414887008));
#43299=CARTESIAN_POINT('Ctrl Pts',(158.973165491318,-2.73519141218658,339.089832880512));
#43300=CARTESIAN_POINT('Ctrl Pts',(158.96541841294,-2.61996806679041,339.164586621901));
#43301=CARTESIAN_POINT('Ctrl Pts',(158.957671334562,-2.50182152122744,339.234391590113));
#43302=CARTESIAN_POINT('Ctrl Pts',(158.949924191257,-2.38367398548289,339.304197143359));
#43303=CARTESIAN_POINT('Ctrl Pts',(158.942177047951,-2.26260353723115,339.369053641872));
#43304=CARTESIAN_POINT('Ctrl Pts',(158.934429904645,-2.13906738459991,339.428721461849));
#43305=CARTESIAN_POINT('Ctrl Pts',(158.926681019617,-2.01550345841856,339.488402696418));
#43306=CARTESIAN_POINT('Ctrl Pts',(158.918932134589,-1.88947307667827,339.542892761229));
#43307=CARTESIAN_POINT('Ctrl Pts',(158.911183249561,-1.76145504787547,339.591999474827));
#43308=CARTESIAN_POINT('Ctrl Pts',(158.903426139786,-1.6333011394143,339.641158310799));
#43309=CARTESIAN_POINT('Ctrl Pts',(158.895669030011,-1.50315573507092,339.684922241206));
#43310=CARTESIAN_POINT('Ctrl Pts',(158.887911920237,-1.3715150195725,339.723148273513));
#43311=CARTESIAN_POINT('Ctrl Pts',(158.88015066531,-1.23980395948498,339.761394732589));
#43312=CARTESIAN_POINT('Ctrl Pts',(158.872389410384,-1.10659637548001,339.794097303796));
#43313=CARTESIAN_POINT('Ctrl Pts',(158.864628155458,-0.972399404108642,
339.821164015193));
#43314=CARTESIAN_POINT('Ctrl Pts',(158.856854485054,-0.837987761317682,
339.848274024507));
#43315=CARTESIAN_POINT('Ctrl Pts',(158.849080814649,-0.702583954722853,
339.869730097086));
#43316=CARTESIAN_POINT('Ctrl Pts',(158.841307144244,-0.566701902813514,
339.885491993223));
#43317=CARTESIAN_POINT('Ctrl Pts',(158.833895340067,-0.437145193110627,
339.900520169303));
#43318=CARTESIAN_POINT('Ctrl Pts',(158.82648353589,-0.307154047705987,339.910372344821));
#43319=CARTESIAN_POINT('Ctrl Pts',(158.819071731713,-0.177172671851662,
339.915057772483));
#43320=CARTESIAN_POINT('Ctrl Pts',(158.811296652934,-0.0408205215732932,
339.919972846913));
#43321=CARTESIAN_POINT('Ctrl Pts',(158.803521574156,0.0959517752568021,
339.919217424385));
#43322=CARTESIAN_POINT('Ctrl Pts',(158.795746495378,0.23263337072655,339.912745136614));
#43323=CARTESIAN_POINT('Ctrl Pts',(158.787980984329,0.369146770791589,339.906280813405));
#43324=CARTESIAN_POINT('Ctrl Pts',(158.78021547328,0.505569304871357,339.894113640831));
#43325=CARTESIAN_POINT('Ctrl Pts',(158.772449962231,0.641387009309717,339.876249149376));
#43326=CARTESIAN_POINT('Ctrl Pts',(158.764692150708,0.777070050098496,339.858402370616));
#43327=CARTESIAN_POINT('Ctrl Pts',(158.756934339186,0.912149069623679,339.834869565268));
#43328=CARTESIAN_POINT('Ctrl Pts',(158.749176527664,1.04611247282728,339.805708247147));
#43329=CARTESIAN_POINT('Ctrl Pts',(158.741424554141,1.17997506432178,339.776568873842));
#43330=CARTESIAN_POINT('Ctrl Pts',(158.733672580618,1.3127233301591,339.741809501391));
#43331=CARTESIAN_POINT('Ctrl Pts',(158.725920607095,1.44385350619738,339.701539121941));
#43332=CARTESIAN_POINT('Ctrl Pts',(158.718171916537,1.57492814852837,339.66128579702));
#43333=CARTESIAN_POINT('Ctrl Pts',(158.71042322598,1.70438569112442,339.615526221602));
#43334=CARTESIAN_POINT('Ctrl Pts',(158.702674535422,1.83173544545043,339.564419822976));
#43335=CARTESIAN_POINT('Ctrl Pts',(158.694927457044,1.95905870359635,339.513324057464));
#43336=CARTESIAN_POINT('Ctrl Pts',(158.687180378667,2.08427468323903,339.456883826972));
#43337=CARTESIAN_POINT('Ctrl Pts',(158.679433300289,2.20691104528425,339.39530734997));
#43338=CARTESIAN_POINT('Ctrl Pts',(158.671686156983,2.32954843514021,339.333730356898));
#43339=CARTESIAN_POINT('Ctrl Pts',(158.663939013677,2.44960581496282,339.267017206849));
#43340=CARTESIAN_POINT('Ctrl Pts',(158.656191870371,2.56663425843017,339.195422701702));
#43341=CARTESIAN_POINT('Ctrl Pts',(158.648442985343,2.6836890123765,339.123812100589));
#43342=CARTESIAN_POINT('Ctrl Pts',(158.640694100315,2.79771314155195,339.047318164551));
#43343=CARTESIAN_POINT('Ctrl Pts',(158.632945215287,2.90828592572085,338.966239533457));
#43344=CARTESIAN_POINT('Ctrl Pts',(158.625188105512,3.01897607298517,338.885074844665));
#43345=CARTESIAN_POINT('Ctrl Pts',(158.617430995737,3.12620724175919,338.799315971539));
#43346=CARTESIAN_POINT('Ctrl Pts',(158.609673885963,3.22959067254162,338.709302784936));
#43347=CARTESIAN_POINT('Ctrl Pts',(158.601912631037,3.33302934812382,338.619241498163));
#43348=CARTESIAN_POINT('Ctrl Pts',(158.59415137611,3.43261590508547,338.524921636667));
#43349=CARTESIAN_POINT('Ctrl Pts',(158.586390121184,3.52799856157159,338.426719891098));
#43350=CARTESIAN_POINT('Ctrl Pts',(158.57861645078,3.62353379922298,338.32836105474));
#43351=CARTESIAN_POINT('Ctrl Pts',(158.570842780375,3.7148514376178,338.226108217083));
#43352=CARTESIAN_POINT('Ctrl Pts',(158.56306910997,3.80163952754342,338.120371767133));
#43353=CARTESIAN_POINT('Ctrl Pts',(158.555657305793,3.88438761100264,338.019557374367));
#43354=CARTESIAN_POINT('Ctrl Pts',(158.548245501616,3.96301818325018,337.915576624448));
#43355=CARTESIAN_POINT('Ctrl Pts',(158.540833697439,4.03729864013467,337.808808066221));
#43356=CARTESIAN_POINT('Ctrl Pts',(158.533058618661,4.11521980348147,337.696806462907));
#43357=CARTESIAN_POINT('Ctrl Pts',(158.525283539882,4.18859989036917,337.581382918117));
#43358=CARTESIAN_POINT('Ctrl Pts',(158.517508461104,4.25712345959927,337.46294192222));
#43359=CARTESIAN_POINT('Ctrl Pts',(158.509742950055,4.32556270621511,337.344646675508));
#43360=CARTESIAN_POINT('Ctrl Pts',(158.501977439006,4.38915713233624,337.223341700921));
#43361=CARTESIAN_POINT('Ctrl Pts',(158.494211927957,4.44763325343954,337.099462194325));
#43362=CARTESIAN_POINT('Ctrl Pts',(158.486454116435,4.5060513952982,336.97570551462));
#43363=CARTESIAN_POINT('Ctrl Pts',(158.478696304912,4.55936116552816,336.849379734031));
#43364=CARTESIAN_POINT('Ctrl Pts',(158.47093849339,4.6073340752823,336.720946187782));
#43365=CARTESIAN_POINT('Ctrl Pts',(158.463186519867,4.65527088390076,336.592609291849));
#43366=CARTESIAN_POINT('Ctrl Pts',(158.455434546344,4.6978786897868,336.462168152121));
#43367=CARTESIAN_POINT('Ctrl Pts',(158.447682572821,4.73497653107848,336.330105376516));
#43368=CARTESIAN_POINT('Ctrl Pts',(158.439933882264,4.77205866141234,336.198098529575));
#43369=CARTESIAN_POINT('Ctrl Pts',(158.432185191706,4.80363536277662,336.064471788207));
#43370=CARTESIAN_POINT('Ctrl Pts',(158.424436501148,4.82957516125823,335.929724058126));
#43371=CARTESIAN_POINT('Ctrl Pts',(158.41668942277,4.85550956274804,335.795004363435));
#43372=CARTESIAN_POINT('Ctrl Pts',(158.408942344393,4.875809320304,335.659164527529));
#43373=CARTESIAN_POINT('Ctrl Pts',(158.401195266015,4.89039391949234,335.52271442939));
#43374=CARTESIAN_POINT('Ctrl Pts',(158.393448122709,4.9049786409137,335.386263187667));
#43375=CARTESIAN_POINT('Ctrl Pts',(158.385700979403,4.91384806688786,335.249202062171));
#43376=CARTESIAN_POINT('Ctrl Pts',(158.377953836097,4.91697352595815,335.112046452539));
#43377=CARTESIAN_POINT('Ctrl Pts',(158.370204951069,4.92009968769801,334.974860007415));
#43378=CARTESIAN_POINT('Ctrl Pts',(158.362456066041,4.91747930395742,334.837579426582));
#43379=CARTESIAN_POINT('Ctrl Pts',(158.354707181013,4.90913583151195,334.700720113831));
#43380=CARTESIAN_POINT('Ctrl Pts',(158.346950071238,4.90078350321865,334.563715537192));
#43381=CARTESIAN_POINT('Ctrl Pts',(158.339192961463,4.88669597556864,334.427133512602));
#43382=CARTESIAN_POINT('Ctrl Pts',(158.331435851689,4.86694867314278,334.291484879841));
#43383=CARTESIAN_POINT('Ctrl Pts',(158.323674596763,4.84719081838988,334.155763760788));
#43384=CARTESIAN_POINT('Ctrl Pts',(158.315913341836,4.82176723487931,334.020977411325));
#43385=CARTESIAN_POINT('Ctrl Pts',(158.30815208691,4.7908043204682,333.887625501244));
#43386=CARTESIAN_POINT('Ctrl Pts',(158.300378416506,4.75979187548484,333.754060271566));
#43387=CARTESIAN_POINT('Ctrl Pts',(158.292604746101,4.72322249677057,333.62193444354));
#43388=CARTESIAN_POINT('Ctrl Pts',(158.284831075696,4.68127247557753,333.491732426955));
#43389=CARTESIAN_POINT('Ctrl Pts',(158.277419271519,4.6412752379636,333.367591345566));
#43390=CARTESIAN_POINT('Ctrl Pts',(158.270007467342,4.59638712148911,333.245199269658));
#43391=CARTESIAN_POINT('Ctrl Pts',(158.262595663165,4.54680058049984,333.124956655523));
#43392=CARTESIAN_POINT('Ctrl Pts',(158.254820584386,4.49478365542606,332.998820592686));
#43393=CARTESIAN_POINT('Ctrl Pts',(158.247045505608,4.43743170972269,332.87465140904));
#43394=CARTESIAN_POINT('Ctrl Pts',(158.23927042683,4.37491418463676,332.752933258765));
#43395=CARTESIAN_POINT('Ctrl Pts',(158.231504915781,4.3124735913456,332.631364890423));
#43396=CARTESIAN_POINT('Ctrl Pts',(158.223739404732,4.24488024330886,332.512241898544));
#43397=CARTESIAN_POINT('Ctrl Pts',(158.215973893683,4.17235210784672,332.396029771551));
#43398=CARTESIAN_POINT('Ctrl Pts',(158.20821608216,4.09989588424172,332.27993286922));
#43399=CARTESIAN_POINT('Ctrl Pts',(158.200458270638,4.02251481588706,332.166741417671));
#43400=CARTESIAN_POINT('Ctrl Pts',(158.192700459116,3.940473200989,332.05689721301));
#43401=CARTESIAN_POINT('Ctrl Pts',(158.184948485593,3.85849332500805,331.947135669597));
#43402=CARTESIAN_POINT('Ctrl Pts',(158.17719651207,3.77186011637104,331.840716671212));
#43403=CARTESIAN_POINT('Ctrl Pts',(158.169444538547,3.68088148152566,331.738053559382));
#43404=CARTESIAN_POINT('Ctrl Pts',(158.161695847989,3.58994137618627,331.635433925441));
#43405=CARTESIAN_POINT('Ctrl Pts',(158.153947157432,3.49465976354808,331.53656730635));
#43406=CARTESIAN_POINT('Ctrl Pts',(158.146198466874,3.39538503598947,331.441834247835));
#43407=CARTESIAN_POINT('Ctrl Pts',(158.138451388496,3.29613096336722,331.347120899325));
#43408=CARTESIAN_POINT('Ctrl Pts',(158.130704310118,3.19288571095138,331.256539670423));
#43409=CARTESIAN_POINT('Ctrl Pts',(158.122957231741,3.08603447587614,331.170434192209));
#43410=CARTESIAN_POINT('Ctrl Pts',(158.115210088435,2.97918234528422,331.084327992347));
#43411=CARTESIAN_POINT('Ctrl Pts',(158.107462945129,2.86872447610553,331.002697863253));
#43412=CARTESIAN_POINT('Ctrl Pts',(158.099715801823,2.75507876312124,330.925846827683));
#43413=CARTESIAN_POINT('Ctrl Pts',(158.091966916795,2.64140750016842,330.848978514369));
#43414=CARTESIAN_POINT('Ctrl Pts',(158.084218031767,2.52454729099416,330.776891651514));
#43415=CARTESIAN_POINT('Ctrl Pts',(158.076469146739,2.40494424344854,330.709845428379));
#43416=CARTESIAN_POINT('Ctrl Pts',(158.068712036964,2.28521424799237,330.642728041689));
#43417=CARTESIAN_POINT('Ctrl Pts',(158.060954927189,2.16273594011134,330.580662173654));
#43418=CARTESIAN_POINT('Ctrl Pts',(158.053197817415,2.03797971244386,330.52386084285));
#43419=CARTESIAN_POINT('Ctrl Pts',(158.045436562489,1.91315681903709,330.467029159232));
#43420=CARTESIAN_POINT('Ctrl Pts',(158.037675307562,1.78605394239045,330.415467765261));
#43421=CARTESIAN_POINT('Ctrl Pts',(158.029914052636,1.6571596666253,330.369340770278));
#43422=CARTESIAN_POINT('Ctrl Pts',(158.022140382232,1.52805920202558,330.323139987136));
#43423=CARTESIAN_POINT('Ctrl Pts',(158.014366711827,1.39716198528526,330.282391090947));
#43424=CARTESIAN_POINT('Ctrl Pts',(158.006593041422,1.26497076824122,330.247207976568));
#43425=CARTESIAN_POINT('Ctrl Pts',(157.999181237245,1.13893308415445,330.213662644629));
#43426=CARTESIAN_POINT('Ctrl Pts',(157.991769433068,1.01171944089938,330.185176644288));
#43427=CARTESIAN_POINT('Ctrl Pts',(157.984357628891,0.883770738806445,330.161804846461));
#43428=CARTESIAN_POINT('Ctrl Pts',(157.976582550113,0.749550889683846,330.137287527201));
#43429=CARTESIAN_POINT('Ctrl Pts',(157.968807471334,0.614097945448172,330.118320931796));
#43430=CARTESIAN_POINT('Ctrl Pts',(157.961032392556,0.477910736060523,330.105024577094));
#43431=CARTESIAN_POINT('Ctrl Pts',(157.953266881507,0.341891113704359,330.091744584403));
#43432=CARTESIAN_POINT('Ctrl Pts',(157.945501370458,0.205139409327207,330.084120986626));
#43433=CARTESIAN_POINT('Ctrl Pts',(157.937735859409,0.0681650167000006,
330.082222392889));
#43434=CARTESIAN_POINT('Ctrl Pts',(157.929978047886,-0.0686735654189404,
330.080325681614));
#43435=CARTESIAN_POINT('Ctrl Pts',(157.922220236364,-0.205734008072243,
330.084142683489));
#43436=CARTESIAN_POINT('Ctrl Pts',(157.914462424842,-0.342501768563146,
330.093690225737));
#43437=CARTESIAN_POINT('Ctrl Pts',(157.906710451319,-0.479166606975382,
330.103230583156));
#43438=CARTESIAN_POINT('Ctrl Pts',(157.898958477796,-0.615538813271953,
330.11849287019));
#43439=CARTESIAN_POINT('Ctrl Pts',(157.891206504273,-0.751104173897883,
330.139441844556));
#43440=CARTESIAN_POINT('Ctrl Pts',(157.883457813716,-0.886612122514278,
330.160381947019));
#43441=CARTESIAN_POINT('Ctrl Pts',(157.875709123158,-1.02131351959116,330.187003887275));
#43442=CARTESIAN_POINT('Ctrl Pts',(157.8679604326,-1.15469982100203,330.219220629868));
#43443=CARTESIAN_POINT('Ctrl Pts',(157.860213354223,-1.28805837027858,330.251430669499));
#43444=CARTESIAN_POINT('Ctrl Pts',(157.852466275845,-1.4201019884216,330.289233104388));
#43445=CARTESIAN_POINT('Ctrl Pts',(157.844719197467,-1.55033325645351,330.332489972541));
#43446=CARTESIAN_POINT('Ctrl Pts',(157.836972054161,-1.68056561594917,330.375747203228));
#43447=CARTESIAN_POINT('Ctrl Pts',(157.829224910855,-1.8089852240907,330.424458835146));
#43448=CARTESIAN_POINT('Ctrl Pts',(157.821477767549,-1.93511111573167,330.478437434661));
#43449=CARTESIAN_POINT('Ctrl Pts',(157.813728882521,-2.06126536314975,330.532428169711));
#43450=CARTESIAN_POINT('Ctrl Pts',(157.805979997493,-2.18512450865172,330.591688074874));
#43451=CARTESIAN_POINT('Ctrl Pts',(157.798231112465,-2.30622917990243,330.655982270724));
#43452=CARTESIAN_POINT('Ctrl Pts',(157.790474002691,-2.42746239290329,330.720344709098));
#43453=CARTESIAN_POINT('Ctrl Pts',(157.782716892916,-2.54593494564991,330.789751928622));
#43454=CARTESIAN_POINT('Ctrl Pts',(157.774959783141,-2.66121314982761,330.863923642668));
#43455=CARTESIAN_POINT('Ctrl Pts',(157.767198528215,-2.77655295499194,330.938134991706));
#43456=CARTESIAN_POINT('Ctrl Pts',(157.759437273289,-2.88869469091162,331.017115683429));
#43457=CARTESIAN_POINT('Ctrl Pts',(157.751676018363,-2.99723595363773,331.100543666007));
#43458=CARTESIAN_POINT('Ctrl Pts',(157.743902347958,-3.10595084701051,331.184105106167));
#43459=CARTESIAN_POINT('Ctrl Pts',(157.736128677553,-3.21105345801417,331.272127802395));
#43460=CARTESIAN_POINT('Ctrl Pts',(157.728355007149,-3.3121759421672,331.364250614986));
#43461=CARTESIAN_POINT('Ctrl Pts',(157.720943202972,-3.40859115035515,331.452085088489));
#43462=CARTESIAN_POINT('Ctrl Pts',(157.713531398794,-3.50138823764749,331.543646345776));
#43463=CARTESIAN_POINT('Ctrl Pts',(157.706119594617,-3.59028246545467,331.638593318156));
#43464=CARTESIAN_POINT('Ctrl Pts',(157.69843538853,-3.68244377330101,331.737029823724));
#43465=CARTESIAN_POINT('Ctrl Pts',(157.690751182442,-3.77071663201147,331.839433621995));
#43466=CARTESIAN_POINT('Ctrl Pts',(157.683066976355,-3.85473394334092,331.945460871333));
#43467=CARTESIAN_POINT('Ctrl Pts',(157.675294862694,-3.9397124155088,332.052701075934));
#43468=CARTESIAN_POINT('Ctrl Pts',(157.667522749033,-4.02033702629779,332.163647915457));
#43469=CARTESIAN_POINT('Ctrl Pts',(157.659750635372,-4.09626487565926,332.277905745397));
#43470=CARTESIAN_POINT('Ctrl Pts',(157.652085329165,-4.1711492945344,332.390593399124));
#43471=CARTESIAN_POINT('Ctrl Pts',(157.644420022959,-4.24146497036335,332.506501287287));
#43472=CARTESIAN_POINT('Ctrl Pts',(157.636754716753,-4.30692271572899,332.625215844916));
#43473=CARTESIAN_POINT('Ctrl Pts',(157.62909448777,-4.37233710423443,332.743851770285));
#43474=CARTESIAN_POINT('Ctrl Pts',(157.621434258788,-4.43289976821759,332.865290318654));
#43475=CARTESIAN_POINT('Ctrl Pts',(157.613774029805,-4.48836528415092,332.989089723899));
#43476=CARTESIAN_POINT('Ctrl Pts',(157.606117122602,-4.54380674803161,333.112835444801));
#43477=CARTESIAN_POINT('Ctrl Pts',(157.598460215399,-4.59415529729811,333.238939620846));
#43478=CARTESIAN_POINT('Ctrl Pts',(157.590803308196,-4.63921210000655,333.36693718625));
#43479=CARTESIAN_POINT('Ctrl Pts',(157.582947719888,-4.68543803473639,333.498256027098));
#43480=CARTESIAN_POINT('Ctrl Pts',(157.575092131579,-4.72609365772853,333.631567466467));
#43481=CARTESIAN_POINT('Ctrl Pts',(157.56723654327,-4.76101761804595,333.766349197238));
#43482=CARTESIAN_POINT('Ctrl Pts',(157.559579005358,-4.79506109635081,333.897732891575));
#43483=CARTESIAN_POINT('Ctrl Pts',(157.551921467446,-4.82365839707103,334.030513215732));
#43484=CARTESIAN_POINT('Ctrl Pts',(157.544263929534,-4.84671133777158,334.164193640359));
#43485=CARTESIAN_POINT('Ctrl Pts',(157.536309316027,-4.87065862155782,334.303060221711));
#43486=CARTESIAN_POINT('Ctrl Pts',(157.528354702519,-4.88862259265559,334.442897688675));
#43487=CARTESIAN_POINT('Ctrl Pts',(157.520400089012,-4.9005522594639,334.583141972893));
#43488=CARTESIAN_POINT('Ctrl Pts',(157.512445475505,-4.91248192627221,334.723386257111));
#43489=CARTESIAN_POINT('Ctrl Pts',(157.504490861997,-4.91837729646438,334.864036875012));
#43490=CARTESIAN_POINT('Ctrl Pts',(157.49653624849,-4.91824791444157,335.004529303609));
#43491=CARTESIAN_POINT('',(160.996536248442,-4.91824826623638,334.995870331392));
#43492=CARTESIAN_POINT('Ctrl Pts',(160.996536248442,-4.91824826623638,334.995870331392));
#43493=CARTESIAN_POINT('Ctrl Pts',(160.988888496737,-4.91836138603388,335.130590886655));
#43494=CARTESIAN_POINT('Ctrl Pts',(160.981240745031,-4.91293495396237,335.265506930197));
#43495=CARTESIAN_POINT('Ctrl Pts',(160.973592993325,-4.90194747536038,335.400117496878));
#43496=CARTESIAN_POINT('Ctrl Pts',(160.965952299152,-4.89097013627331,335.534603841624));
#43497=CARTESIAN_POINT('Ctrl Pts',(160.958311604979,-4.87444199050219,335.668784870466));
#43498=CARTESIAN_POINT('Ctrl Pts',(160.950670910806,-4.85239359350145,335.802159258655));
#43499=CARTESIAN_POINT('Ctrl Pts',(160.943007038341,-4.8302783119756,335.935938242363));
#43500=CARTESIAN_POINT('Ctrl Pts',(160.935343165875,-4.80260923420165,336.068905274069));
#43501=CARTESIAN_POINT('Ctrl Pts',(160.927679293409,-4.76946974119217,336.200558807536));
#43502=CARTESIAN_POINT('Ctrl Pts',(160.920045957973,-4.73646229391907,336.331687761832));
#43503=CARTESIAN_POINT('Ctrl Pts',(160.912412622537,-4.69802804746684,336.461513272552));
#43504=CARTESIAN_POINT('Ctrl Pts',(160.904779287102,-4.65430054956791,336.589550079989));
#43505=CARTESIAN_POINT('Ctrl Pts',(160.897146710172,-4.61057739676862,336.717574164706));
#43506=CARTESIAN_POINT('Ctrl Pts',(160.889514133243,-4.5615621687742,336.843809517671));
#43507=CARTESIAN_POINT('Ctrl Pts',(160.881881556314,-4.50743792766208,336.967787181271));
#43508=CARTESIAN_POINT('Ctrl Pts',(160.874247971392,-4.45330653865675,337.091781217924));
#43509=CARTESIAN_POINT('Ctrl Pts',(160.86661438647,-4.39406495682902,337.213516602669));
#43510=CARTESIAN_POINT('Ctrl Pts',(160.858980801548,-4.32994368055142,337.332545987918));
#43511=CARTESIAN_POINT('Ctrl Pts',(160.851293899055,-4.26537454252244,337.452406746341));
#43512=CARTESIAN_POINT('Ctrl Pts',(160.843606996562,-4.1958574744717,337.569523191195));
#43513=CARTESIAN_POINT('Ctrl Pts',(160.835920094069,-4.12167339589594,337.683466318042));
#43514=CARTESIAN_POINT('Ctrl Pts',(160.828275344467,-4.04789612271273,337.796784611644));
#43515=CARTESIAN_POINT('Ctrl Pts',(160.820630594865,-3.96950318168107,337.906964009669));
#43516=CARTESIAN_POINT('Ctrl Pts',(160.812985845263,-3.88681216102772,338.013614820674));
#43517=CARTESIAN_POINT('Ctrl Pts',(160.805277866324,-3.8034372071318,338.121147735134));
#43518=CARTESIAN_POINT('Ctrl Pts',(160.797569887385,-3.71569303168184,338.225093115699));
#43519=CARTESIAN_POINT('Ctrl Pts',(160.789861908447,-3.62394324269666,338.325089237331));
#43520=CARTESIAN_POINT('Ctrl Pts',(160.782153929508,-3.53219345371147,338.425085358962));
#43521=CARTESIAN_POINT('Ctrl Pts',(160.774445950569,-3.43643838960118,338.521131976034));
#43522=CARTESIAN_POINT('Ctrl Pts',(160.766737971631,-3.33707505998658,338.612909230318));
#43523=CARTESIAN_POINT('Ctrl Pts',(160.758962892852,-3.23684674831298,338.705485428021));
#43524=CARTESIAN_POINT('Ctrl Pts',(160.751187814074,-3.13260480339346,338.794033995275));
#43525=CARTESIAN_POINT('Ctrl Pts',(160.743412735296,-3.02470651911524,338.878186887673));
#43526=CARTESIAN_POINT('Ctrl Pts',(160.735647224247,-2.91694101054498,338.96223622458));
#43527=CARTESIAN_POINT('Ctrl Pts',(160.727881713198,-2.80552842031864,339.041900411215));
#43528=CARTESIAN_POINT('Ctrl Pts',(160.720116202149,-2.69086222332686,339.116848741158));
#43529=CARTESIAN_POINT('Ctrl Pts',(160.712358390626,-2.5763097182034,339.191722759613));
#43530=CARTESIAN_POINT('Ctrl Pts',(160.704600579104,-2.45851035123436,339.261890013978));
#43531=CARTESIAN_POINT('Ctrl Pts',(160.696842767582,-2.33788967322245,339.32706077359));
#43532=CARTESIAN_POINT('Ctrl Pts',(160.689090794059,-2.21735976609566,339.392182490138));
#43533=CARTESIAN_POINT('Ctrl Pts',(160.681338820536,-2.09401311640985,339.452315011018));
#43534=CARTESIAN_POINT('Ctrl Pts',(160.673586847013,-1.96830287833509,339.50721275753));
#43535=CARTESIAN_POINT('Ctrl Pts',(160.665838156455,-1.84264587862081,339.562087254813));
#43536=CARTESIAN_POINT('Ctrl Pts',(160.658089465898,-1.71462763886035,339.611731230944));
#43537=CARTESIAN_POINT('Ctrl Pts',(160.65034077534,-1.58472425844211,339.655945885339));
#43538=CARTESIAN_POINT('Ctrl Pts',(160.642593696962,-1.45484790550707,339.700151340506));
#43539=CARTESIAN_POINT('Ctrl Pts',(160.634846618585,-1.32308756186165,339.738929594957));
#43540=CARTESIAN_POINT('Ctrl Pts',(160.627099540207,-1.18993720038836,339.772130815645));
#43541=CARTESIAN_POINT('Ctrl Pts',(160.619352396901,-1.05678572298708,339.805332314592));
#43542=CARTESIAN_POINT('Ctrl Pts',(160.611605253595,-0.922244583783325,
339.832956591977));
#43543=CARTESIAN_POINT('Ctrl Pts',(160.603858110289,-0.786820349727822,
339.854904406861));
#43544=CARTESIAN_POINT('Ctrl Pts',(160.596109225261,-0.651365669429618,
339.876857156079));
#43545=CARTESIAN_POINT('Ctrl Pts',(160.588360340233,-0.515027884974828,
339.893130840803));
#43546=CARTESIAN_POINT('Ctrl Pts',(160.580611455205,-0.378320732445168,
339.90367785299));
#43547=CARTESIAN_POINT('Ctrl Pts',(160.57285434543,-0.241468477530827,339.914236059884));
#43548=CARTESIAN_POINT('Ctrl Pts',(160.565097235656,-0.104246461714505,
339.919055422054));
#43549=CARTESIAN_POINT('Ctrl Pts',(160.557340125881,0.0328289566454363,
339.918140433345));
#43550=CARTESIAN_POINT('Ctrl Pts',(160.549578870955,0.169977623725964,339.917224955695));
#43551=CARTESIAN_POINT('Ctrl Pts',(160.541817616029,0.306979147040823,339.910569040322));
#43552=CARTESIAN_POINT('Ctrl Pts',(160.534056361103,0.443321225932666,339.89822920586));
#43553=CARTESIAN_POINT('Ctrl Pts',(160.526282690698,0.579881407717048,339.885869631683));
#43554=CARTESIAN_POINT('Ctrl Pts',(160.518509020293,0.715779649412491,339.867808020597));
#43555=CARTESIAN_POINT('Ctrl Pts',(160.510735349889,0.850511907688802,339.844152408562));
#43556=CARTESIAN_POINT('Ctrl Pts',(160.503323545711,0.978972346929401,339.821597970959));
#43557=CARTESIAN_POINT('Ctrl Pts',(160.495911741534,1.10637263163476,339.7939586746));
#43558=CARTESIAN_POINT('Ctrl Pts',(160.488499937357,1.23228965352745,339.76137010453));
#43559=CARTESIAN_POINT('Ctrl Pts',(160.480724858579,1.3643782437488,339.727184271565));
#43560=CARTESIAN_POINT('Ctrl Pts',(160.4729497798,1.49525192085116,339.687443706834));
#43561=CARTESIAN_POINT('Ctrl Pts',(160.465174701022,1.6244078362171,339.642249696444));
#43562=CARTESIAN_POINT('Ctrl Pts',(160.457409189973,1.75340481700674,339.597111300161));
#43563=CARTESIAN_POINT('Ctrl Pts',(160.449643678924,1.88068787653359,339.546532938675));
#43564=CARTESIAN_POINT('Ctrl Pts',(160.441878167875,2.00576598487248,339.490666529195));
#43565=CARTESIAN_POINT('Ctrl Pts',(160.434120356352,2.13072007790309,339.434855511422));
#43566=CARTESIAN_POINT('Ctrl Pts',(160.42636254483,2.25347321584484,339.373767038131));
#43567=CARTESIAN_POINT('Ctrl Pts',(160.418604733308,2.37355146804535,339.307602174185));
#43568=CARTESIAN_POINT('Ctrl Pts',(160.410852759785,2.49353935755304,339.241487101396));
#43569=CARTESIAN_POINT('Ctrl Pts',(160.403100786262,2.61085602700582,339.170303429641));
#43570=CARTESIAN_POINT('Ctrl Pts',(160.395348812739,2.7250497363142,339.094299329203));
#43571=CARTESIAN_POINT('Ctrl Pts',(160.387600122181,2.83919508451884,339.018327416547));
#43572=CARTESIAN_POINT('Ctrl Pts',(160.379851431624,2.95021977837428,338.937539351638));
#43573=CARTESIAN_POINT('Ctrl Pts',(160.372102741066,3.05769899753217,338.852227914206));
#43574=CARTESIAN_POINT('Ctrl Pts',(160.364355662688,3.16515585474074,338.766934226532));
#43575=CARTESIAN_POINT('Ctrl Pts',(160.35660858431,3.26906839856009,338.677119281156));
#43576=CARTESIAN_POINT('Ctrl Pts',(160.348861505933,3.36904331411287,338.583117387155));
#43577=CARTESIAN_POINT('Ctrl Pts',(160.341114362627,3.46901906755175,338.489114705327));
#43578=CARTESIAN_POINT('Ctrl Pts',(160.333367219321,3.56505684213524,338.390925272635));
#43579=CARTESIAN_POINT('Ctrl Pts',(160.325620076015,3.65679905159574,338.288921367067));
#43580=CARTESIAN_POINT('Ctrl Pts',(160.317871190987,3.74856188665252,338.186894528855));
#43581=CARTESIAN_POINT('Ctrl Pts',(160.310122305959,3.83602697354957,338.081051801856));
#43582=CARTESIAN_POINT('Ctrl Pts',(160.302373420931,3.91887626559672,337.971799434256));
#43583=CARTESIAN_POINT('Ctrl Pts',(160.294616311156,4.00181349473862,337.862431105064));
#43584=CARTESIAN_POINT('Ctrl Pts',(160.286859201381,4.08012490575982,337.749646217865));
#43585=CARTESIAN_POINT('Ctrl Pts',(160.279102091607,4.1535348464942,337.633881421298));
#43586=CARTESIAN_POINT('Ctrl Pts',(160.27134083668,4.22698401515371,337.518054763725));
#43587=CARTESIAN_POINT('Ctrl Pts',(160.263579581754,4.29552629933025,337.399245362245));
#43588=CARTESIAN_POINT('Ctrl Pts',(160.255818326828,4.35893199146693,337.277914606886));
#43589=CARTESIAN_POINT('Ctrl Pts',(160.248044656423,4.4224391120471,337.156389761861));
#43590=CARTESIAN_POINT('Ctrl Pts',(160.240270986019,4.48079305437756,337.032335857023));
#43591=CARTESIAN_POINT('Ctrl Pts',(160.232497315614,4.53381190143574,336.906235217621));
#43592=CARTESIAN_POINT('Ctrl Pts',(160.225085511437,4.58436270840709,336.786004593323));
#43593=CARTESIAN_POINT('Ctrl Pts',(160.21767370726,4.63006383871998,336.663913766749));
#43594=CARTESIAN_POINT('Ctrl Pts',(160.210261903083,4.67080034056367,336.540391911525));
#43595=CARTESIAN_POINT('Ctrl Pts',(160.202486824305,4.71353345971103,336.410815882221));
#43596=CARTESIAN_POINT('Ctrl Pts',(160.194711745526,4.75093802721173,336.279255515189));
#43597=CARTESIAN_POINT('Ctrl Pts',(160.186936666748,4.78282709647227,336.146188478284));
#43598=CARTESIAN_POINT('Ctrl Pts',(160.179171155699,4.814676924203,336.013285188838));
#43599=CARTESIAN_POINT('Ctrl Pts',(160.17140564465,4.84102466799748,335.878879295031));
#43600=CARTESIAN_POINT('Ctrl Pts',(160.163640133601,4.86173235381075,335.74346592552));
#43601=CARTESIAN_POINT('Ctrl Pts',(160.155882322079,4.88241950789321,335.60818681876));
#43602=CARTESIAN_POINT('Ctrl Pts',(160.148124510556,4.89747767395135,335.471902608088));
#43603=CARTESIAN_POINT('Ctrl Pts',(160.140366699034,4.90681946064763,335.335120639635));
#43604=CARTESIAN_POINT('Ctrl Pts',(160.132614725511,4.91615421735313,335.198441603952));
#43605=CARTESIAN_POINT('Ctrl Pts',(160.124862751988,4.9197811306071,335.061265944464));
#43606=CARTESIAN_POINT('Ctrl Pts',(160.117110778465,4.91766442961309,334.92410783823));
#43607=CARTESIAN_POINT('Ctrl Pts',(160.109362087908,4.9155486250432,334.787007818535));
#43608=CARTESIAN_POINT('Ctrl Pts',(160.10161339735,4.90769405016423,334.649925727324));
#43609=CARTESIAN_POINT('Ctrl Pts',(160.093864706792,4.8941170150312,334.513377245002));
#43610=CARTESIAN_POINT('Ctrl Pts',(160.086117628415,4.88054280471372,334.376857172732));
#43611=CARTESIAN_POINT('Ctrl Pts',(160.078370550037,4.86124854099071,334.240870877234));
#43612=CARTESIAN_POINT('Ctrl Pts',(160.070623471659,4.83630250624762,334.105930019203));
#43613=CARTESIAN_POINT('Ctrl Pts',(160.062876328353,4.81135626243274,333.970988030237));
#43614=CARTESIAN_POINT('Ctrl Pts',(160.055129185047,4.78075822417572,333.837091880575));
#43615=CARTESIAN_POINT('Ctrl Pts',(160.047382041741,4.7446279375319,333.70474373312));
#43616=CARTESIAN_POINT('Ctrl Pts',(160.039633156713,4.70848952803252,333.572365830991));
#43617=CARTESIAN_POINT('Ctrl Pts',(160.031884271685,4.66681649810859,333.441537000599));
#43618=CARTESIAN_POINT('Ctrl Pts',(160.024135386657,4.61977835721469,333.312744538397));
#43619=CARTESIAN_POINT('Ctrl Pts',(160.016378276882,4.57269028955213,333.183815374544));
#43620=CARTESIAN_POINT('Ctrl Pts',(160.008621167108,4.52022586975861,333.056927264257));
#43621=CARTESIAN_POINT('Ctrl Pts',(160.000864057333,4.46260311378447,332.932548304956));
#43622=CARTESIAN_POINT('Ctrl Pts',(159.993102802407,4.40494956605198,332.808102881516));
#43623=CARTESIAN_POINT('Ctrl Pts',(159.985341547481,4.34213236858375,332.686169628044));
#43624=CARTESIAN_POINT('Ctrl Pts',(159.977580292554,4.27441520615785,332.567191395143));
#43625=CARTESIAN_POINT('Ctrl Pts',(159.96980662215,4.20658971834105,332.448022835845));
#43626=CARTESIAN_POINT('Ctrl Pts',(159.962032951745,4.13384880973275,332.331819074693));
#43627=CARTESIAN_POINT('Ctrl Pts',(159.95425928134,4.05649963218452,332.218994103461));
#43628=CARTESIAN_POINT('Ctrl Pts',(159.946847477163,3.98275107745958,332.111421161782));
#43629=CARTESIAN_POINT('Ctrl Pts',(159.939435672986,3.90481380064109,332.00691975448));
#43630=CARTESIAN_POINT('Ctrl Pts',(159.932023868809,3.82298649596497,331.905818797457));
#43631=CARTESIAN_POINT('Ctrl Pts',(159.924248790031,3.73714859133651,331.799762581368));
#43632=CARTESIAN_POINT('Ctrl Pts',(159.916473711252,3.64675842973054,331.697113419032));
#43633=CARTESIAN_POINT('Ctrl Pts',(159.908698632474,3.55211652470703,331.598287011313));
#43634=CARTESIAN_POINT('Ctrl Pts',(159.900933121425,3.45759108257287,331.49958221578));
#43635=CARTESIAN_POINT('Ctrl Pts',(159.893167610376,3.35882457504668,331.404691094571));
#43636=CARTESIAN_POINT('Ctrl Pts',(159.885402099327,3.25615870070829,331.313997615532));
#43637=CARTESIAN_POINT('Ctrl Pts',(159.877644287804,3.15359461988362,331.223394059342));
#43638=CARTESIAN_POINT('Ctrl Pts',(159.869886476282,3.04713915732539,331.136980119872));
#43639=CARTESIAN_POINT('Ctrl Pts',(159.86212866476,2.93717165875148,331.055103840463));
#43640=CARTESIAN_POINT('Ctrl Pts',(159.854376691237,2.827286914207,330.973289175551));
#43641=CARTESIAN_POINT('Ctrl Pts',(159.846624717714,2.71389570650215,330.896005606332));
#43642=CARTESIAN_POINT('Ctrl Pts',(159.838872744191,2.59741106046541,330.823561463942));
#43643=CARTESIAN_POINT('Ctrl Pts',(159.831124053633,2.48097574574546,330.751148001689));
#43644=CARTESIAN_POINT('Ctrl Pts',(159.823375363076,2.36144992956506,330.683570095951));
#43645=CARTESIAN_POINT('Ctrl Pts',(159.815626672518,2.23927608488586,330.621093095514));
#43646=CARTESIAN_POINT('Ctrl Pts',(159.80787959414,2.11712765949555,330.558629093938));
#43647=CARTESIAN_POINT('Ctrl Pts',(159.800132515762,1.99233264926582,330.501264064542));
#43648=CARTESIAN_POINT('Ctrl Pts',(159.792385437385,1.86535827210762,330.449217476172));
#43649=CARTESIAN_POINT('Ctrl Pts',(159.784638294079,1.73838283078182,330.397170451602));
#43650=CARTESIAN_POINT('Ctrl Pts',(159.776891150773,1.60922834776634,330.350442105211));
#43651=CARTESIAN_POINT('Ctrl Pts',(159.769144007467,1.47838179578895,330.309203657333));
#43652=CARTESIAN_POINT('Ctrl Pts',(159.761395122439,1.34750582672902,330.267955938176));
#43653=CARTESIAN_POINT('Ctrl Pts',(159.753646237411,1.21493740445249,330.232200691013));
#43654=CARTESIAN_POINT('Ctrl Pts',(159.745897352383,1.0811780382342,330.202059075797));
#43655=CARTESIAN_POINT('Ctrl Pts',(159.738140242608,0.947276698442352,330.17188546796));
#43656=CARTESIAN_POINT('Ctrl Pts',(159.730383132833,0.812182271505018,330.147337480529));
#43657=CARTESIAN_POINT('Ctrl Pts',(159.722626023059,0.676406371469306,330.128485093615));
#43658=CARTESIAN_POINT('Ctrl Pts',(159.714864768133,0.54055791713391,330.109622632587));
#43659=CARTESIAN_POINT('Ctrl Pts',(159.707103513206,0.404027652957149,330.096461874102));
#43660=CARTESIAN_POINT('Ctrl Pts',(159.69934225828,0.267330676423168,330.089020731876));
#43661=CARTESIAN_POINT('Ctrl Pts',(159.691568587876,0.130415029276243,330.081567686248));
#43662=CARTESIAN_POINT('Ctrl Pts',(159.683794917471,-0.00666747209512181,
330.079852545226));
#43663=CARTESIAN_POINT('Ctrl Pts',(159.676021247066,-0.143402475685821,
330.08384105297));
#43664=CARTESIAN_POINT('Ctrl Pts',(159.668609442889,-0.273772431963202,
330.087643894718));
#43665=CARTESIAN_POINT('Ctrl Pts',(159.661197638712,-0.403826227329201,
330.096631305733));
#43666=CARTESIAN_POINT('Ctrl Pts',(159.653785834535,-0.533125628792797,
330.110730102927));
#43667=CARTESIAN_POINT('Ctrl Pts',(159.646010755756,-0.668762379084622,
330.12551992417));
#43668=CARTESIAN_POINT('Ctrl Pts',(159.638235676978,-0.803997552647739,
330.145981587706));
#43669=CARTESIAN_POINT('Ctrl Pts',(159.6304605982,-0.938318952627116,330.172087344862));
#43670=CARTESIAN_POINT('Ctrl Pts',(159.622695087151,-1.07247506157325,330.198160977222));
#43671=CARTESIAN_POINT('Ctrl Pts',(159.614929576102,-1.20571925425497,330.229864809954));
#43672=CARTESIAN_POINT('Ctrl Pts',(159.607164065053,-1.33754373121088,330.267119288467));
#43673=CARTESIAN_POINT('Ctrl Pts',(159.59940625353,-1.46923750381394,330.304336829056));
#43674=CARTESIAN_POINT('Ctrl Pts',(159.591648442008,-1.59951398827963,330.347093957571));
#43675=CARTESIAN_POINT('Ctrl Pts',(159.583890630486,-1.72787522180085,330.395260020328));
#43676=CARTESIAN_POINT('Ctrl Pts',(159.576138656963,-1.85613985942228,330.443389836595));
#43677=CARTESIAN_POINT('Ctrl Pts',(159.56838668344,-1.98249175042594,330.496920348415));
#43678=CARTESIAN_POINT('Ctrl Pts',(159.560634709917,-2.10644810114723,330.555671090066));
#43679=CARTESIAN_POINT('Ctrl Pts',(159.552886019359,-2.23035195628102,330.614396950744));
#43680=CARTESIAN_POINT('Ctrl Pts',(159.545137328802,-2.35186193645208,330.678338477128));
#43681=CARTESIAN_POINT('Ctrl Pts',(159.537388638244,-2.47051545669817,330.747267179717));
#43682=CARTESIAN_POINT('Ctrl Pts',(159.529641559866,-2.58914429008816,330.816181541113));
#43683=CARTESIAN_POINT('Ctrl Pts',(159.521894481488,-2.70491750790789,330.890080818589));
#43684=CARTESIAN_POINT('Ctrl Pts',(159.514147403111,-2.81739771570163,330.968690885821));
#43685=CARTESIAN_POINT('Ctrl Pts',(159.506400259805,-2.92987886618784,331.047301611882));
#43686=CARTESIAN_POINT('Ctrl Pts',(159.498653116499,-3.03906663121529,331.130622982536));
#43687=CARTESIAN_POINT('Ctrl Pts',(159.490905973193,-3.1445534990683,331.218338149173));
#43688=CARTESIAN_POINT('Ctrl Pts',(159.483157088165,-3.2500640826087,331.306073036043));
#43689=CARTESIAN_POINT('Ctrl Pts',(159.475408203137,-3.35187181282146,331.398203434683));
#43690=CARTESIAN_POINT('Ctrl Pts',(159.467659318109,-3.44960340827078,331.494373181848));
#43691=CARTESIAN_POINT('Ctrl Pts',(159.459902208334,-3.54743873704552,331.590645004577));
#43692=CARTESIAN_POINT('Ctrl Pts',(159.452145098559,-3.64118900951678,331.69096446574));
#43693=CARTESIAN_POINT('Ctrl Pts',(159.444387988785,-3.73051851420033,331.794939208422));
#43694=CARTESIAN_POINT('Ctrl Pts',(159.436626733858,-3.81989575371496,331.898969511883));
#43695=CARTESIAN_POINT('Ctrl Pts',(159.428865478932,-3.90484727634865,332.006658682194));
#43696=CARTESIAN_POINT('Ctrl Pts',(159.421104224006,-3.98507926926955,332.117583257033));
#43697=CARTESIAN_POINT('Ctrl Pts',(159.413330553601,-4.06543960723152,332.228685275041));
#43698=CARTESIAN_POINT('Ctrl Pts',(159.405556883197,-4.14106511319184,332.343032713749));
#43699=CARTESIAN_POINT('Ctrl Pts',(159.397783212792,-4.21170624823518,332.460174505783));
#43700=CARTESIAN_POINT('Ctrl Pts',(159.390371408615,-4.27905902144712,332.571863319214));
#43701=CARTESIAN_POINT('Ctrl Pts',(159.382959604438,-4.34188088694468,332.686091934111));
#43702=CARTESIAN_POINT('Ctrl Pts',(159.375547800261,-4.39999623292924,332.802452227434));
#43703=CARTESIAN_POINT('Ctrl Pts',(159.367226760812,-4.46524081777695,332.933086897193));
#43704=CARTESIAN_POINT('Ctrl Pts',(159.358905721363,-4.52473714990775,333.066776016648));
#43705=CARTESIAN_POINT('Ctrl Pts',(159.350584681915,-4.57820922808688,333.203007143487));
#43706=CARTESIAN_POINT('Ctrl Pts',(159.341913979133,-4.63392828817218,333.344962919292));
#43707=CARTESIAN_POINT('Ctrl Pts',(159.333243276352,-4.68310559610706,333.489678738939));
#43708=CARTESIAN_POINT('Ctrl Pts',(159.32457257357,-4.72548118704292,333.636544605275));
#43709=CARTESIAN_POINT('Ctrl Pts',(159.316291958506,-4.76595033533406,333.776803098252));
#43710=CARTESIAN_POINT('Ctrl Pts',(159.308011343441,-4.80021621604412,333.919022072236));
#43711=CARTESIAN_POINT('Ctrl Pts',(159.299730728377,-4.82810048408559,334.06264799671));
#43712=CARTESIAN_POINT('Ctrl Pts',(159.291464605672,-4.85593595033821,334.206022553565));
#43713=CARTESIAN_POINT('Ctrl Pts',(159.283198482967,-4.87741200318246,334.350798854617));
#43714=CARTESIAN_POINT('Ctrl Pts',(159.274932360262,-4.89240012795802,334.496408845931));
#43715=CARTESIAN_POINT('Ctrl Pts',(159.266685408795,-4.90735349146548,334.641681130693));
#43716=CARTESIAN_POINT('Ctrl Pts',(159.258438457328,-4.91584889819635,334.78778294644));
#43717=CARTESIAN_POINT('Ctrl Pts',(159.250191505861,-4.91780897882096,334.934137185545));
#43718=CARTESIAN_POINT('Ctrl Pts',(159.248973086752,-4.91809856457844,334.955759818134));
#43719=CARTESIAN_POINT('Ctrl Pts',(159.247754667644,-4.91824559059081,334.97738794205));
#43720=CARTESIAN_POINT('Ctrl Pts',(159.246536248535,-4.91824990229953,334.999019678274));
#43721=CARTESIAN_POINT('',(162.746536248527,-4.91824899084518,335.003150642852));
#43722=CARTESIAN_POINT('Ctrl Pts',(162.74653624849,-4.91824899084476,335.003150643507));
#43723=CARTESIAN_POINT('Ctrl Pts',(162.735825569509,-4.91812835470727,335.191467271566));
#43724=CARTESIAN_POINT('Ctrl Pts',(162.725114890528,-4.90719245495907,335.379437381484));
#43725=CARTESIAN_POINT('Ctrl Pts',(162.714404211548,-4.88555668033054,335.566143962061));
#43726=CARTESIAN_POINT('Ctrl Pts',(162.706629132769,-4.86985087377294,335.701677701338));
#43727=CARTESIAN_POINT('Ctrl Pts',(162.698854053991,-4.84847606729068,335.836771555718));
#43728=CARTESIAN_POINT('Ctrl Pts',(162.691078975213,-4.82146346917885,335.970913527496));
#43729=CARTESIAN_POINT('Ctrl Pts',(162.683313464164,-4.79448411178871,336.104890429037));
#43730=CARTESIAN_POINT('Ctrl Pts',(162.675547953115,-4.76188084315117,336.237917399112));
#43731=CARTESIAN_POINT('Ctrl Pts',(162.667782442066,-4.72373664658983,336.369487187295));
#43732=CARTESIAN_POINT('Ctrl Pts',(162.660024630544,-4.68563027011051,336.500926523649));
#43733=CARTESIAN_POINT('Ctrl Pts',(162.652266819021,-4.6419940069098,336.630911180349));
#43734=CARTESIAN_POINT('Ctrl Pts',(162.644509007499,-4.59296187178296,336.758944088608));
#43735=CARTESIAN_POINT('Ctrl Pts',(162.636757033976,-4.54396663489257,336.886880648044));
#43736=CARTESIAN_POINT('Ctrl Pts',(162.629005060453,-4.48958374765954,337.012868018967));
#43737=CARTESIAN_POINT('Ctrl Pts',(162.62125308693,-4.42999693330044,337.136424637905));
#43738=CARTESIAN_POINT('Ctrl Pts',(162.613504396373,-4.3704353539926,337.259928930542));
#43739=CARTESIAN_POINT('Ctrl Pts',(162.605755705815,-4.30567440033075,337.381004167309));
#43740=CARTESIAN_POINT('Ctrl Pts',(162.598007015257,-4.23594568169184,337.49918931741));
#43741=CARTESIAN_POINT('Ctrl Pts',(162.59025993688,-4.16623147069527,337.617349878103));
#43742=CARTESIAN_POINT('Ctrl Pts',(162.582512858502,-4.09155174909183,337.732621211734));
#43743=CARTESIAN_POINT('Ctrl Pts',(162.574765780124,-4.01218359185996,337.844567785747));
#43744=CARTESIAN_POINT('Ctrl Pts',(162.567018636818,-3.93281476944641,337.95651529798));
#43745=CARTESIAN_POINT('Ctrl Pts',(162.559271493512,-3.84875765910029,338.065137676152));
#43746=CARTESIAN_POINT('Ctrl Pts',(162.551524350206,-3.76033185523241,338.170029558383));
#43747=CARTESIAN_POINT('Ctrl Pts',(162.543775465178,-3.67188617136659,338.274945022537));
#43748=CARTESIAN_POINT('Ctrl Pts',(162.53602658015,-3.57907009144691,338.376128023051));
#43749=CARTESIAN_POINT('Ctrl Pts',(162.528277695122,-3.48224229237244,338.473207693144));
#43750=CARTESIAN_POINT('Ctrl Pts',(162.520520585347,-3.38531171927157,338.570390404601));
#43751=CARTESIAN_POINT('Ctrl Pts',(162.512763475573,-3.28436119756791,338.663460808298));
#43752=CARTESIAN_POINT('Ctrl Pts',(162.505006365798,-3.17978534319233,338.752085851059));
#43753=CARTESIAN_POINT('Ctrl Pts',(162.497245110872,-3.07515360682391,338.84075825221));
#43754=CARTESIAN_POINT('Ctrl Pts',(162.489483855946,-2.96689298596905,338.924980319224));
#43755=CARTESIAN_POINT('Ctrl Pts',(162.481722601019,-2.85542891820251,339.004461106765));
#43756=CARTESIAN_POINT('Ctrl Pts',(162.473948930615,-2.74378654425357,339.084069037663));
#43757=CARTESIAN_POINT('Ctrl Pts',(162.46617526021,-2.62893081082613,339.158920319481));
#43758=CARTESIAN_POINT('Ctrl Pts',(162.458401589805,-2.51131446081569,339.228768466279));
#43759=CARTESIAN_POINT('Ctrl Pts',(162.450989785628,-2.39917318019426,339.29536516504));
#43760=CARTESIAN_POINT('Ctrl Pts',(162.443577981451,-2.28452276557371,339.357413901315));
#43761=CARTESIAN_POINT('Ctrl Pts',(162.436166177274,-2.16777251706213,339.414741824475));
#43762=CARTESIAN_POINT('Ctrl Pts',(162.428391098496,-2.04529999109075,339.47487955992));
#43763=CARTESIAN_POINT('Ctrl Pts',(162.420616019717,-1.92012955256796,339.530012065426));
#43764=CARTESIAN_POINT('Ctrl Pts',(162.412840940939,-1.79270863988575,339.579888513379));
#43765=CARTESIAN_POINT('Ctrl Pts',(162.40507542989,-1.66544452674867,339.629703585187));
#43766=CARTESIAN_POINT('Ctrl Pts',(162.397309918841,-1.53593581017178,339.674275327623));
#43767=CARTESIAN_POINT('Ctrl Pts',(162.389544407792,-1.40465395489751,339.713399020823));
#43768=CARTESIAN_POINT('Ctrl Pts',(162.381786596269,-1.27350226596498,339.752483922766));
#43769=CARTESIAN_POINT('Ctrl Pts',(162.374028784747,-1.14058130917899,339.78613141436));
#43770=CARTESIAN_POINT('Ctrl Pts',(162.366270973225,-1.00638160338075,339.814185199063));
#43771=CARTESIAN_POINT('Ctrl Pts',(162.358518999702,-0.872282887116861,
339.842217872403));
#43772=CARTESIAN_POINT('Ctrl Pts',(162.350767026179,-0.73690771831346,339.864665137881));
#43773=CARTESIAN_POINT('Ctrl Pts',(162.343015052656,-0.600760477143031,
339.881420890643));
#43774=CARTESIAN_POINT('Ctrl Pts',(162.335266362098,-0.464670894410022,
339.898169547333));
#43775=CARTESIAN_POINT('Ctrl Pts',(162.327517671541,-0.327810276776393,
339.909231437694));
#43776=CARTESIAN_POINT('Ctrl Pts',(162.319768980983,-0.190691651998446,
339.914551836776));
#43777=CARTESIAN_POINT('Ctrl Pts',(162.312021902605,-0.0536015558956443,
339.919871128904));
#43778=CARTESIAN_POINT('Ctrl Pts',(162.304274824228,0.0837460502419204,
339.919451290681));
#43779=CARTESIAN_POINT('Ctrl Pts',(162.29652774585,0.220834976626965,339.913289628711));
#43780=CARTESIAN_POINT('Ctrl Pts',(162.288780602544,0.357925051949207,339.9071279151));
#43781=CARTESIAN_POINT('Ctrl Pts',(162.281033459238,0.494756052714651,339.895224299309));
#43782=CARTESIAN_POINT('Ctrl Pts',(162.273286315932,0.630814150597845,339.877628170526));
#43783=CARTESIAN_POINT('Ctrl Pts',(162.265537430904,0.766902837229969,339.860028085759));
#43784=CARTESIAN_POINT('Ctrl Pts',(162.257788545876,0.902217887636804,339.836732991467));
#43785=CARTESIAN_POINT('Ctrl Pts',(162.250039660848,1.036253331379,339.807843809412));
#43786=CARTESIAN_POINT('Ctrl Pts',(162.242282551073,1.17043104172609,339.778923964081));
#43787=CARTESIAN_POINT('Ctrl Pts',(162.234525441299,1.30332604959777,339.744398252514));
#43788=CARTESIAN_POINT('Ctrl Pts',(162.226768331524,1.43444473415226,339.704418281484));
#43789=CARTESIAN_POINT('Ctrl Pts',(162.219007076598,1.56563348433942,339.664416946436));
#43790=CARTESIAN_POINT('Ctrl Pts',(162.211245821671,1.69504365122858,339.618955673842));
#43791=CARTESIAN_POINT('Ctrl Pts',(162.203484566745,1.82220034399506,339.568234776021));
#43792=CARTESIAN_POINT('Ctrl Pts',(162.195710896341,1.94956044602968,339.517432741292));
#43793=CARTESIAN_POINT('Ctrl Pts',(162.187937225936,2.07465951357069,339.461354428271));
#43794=CARTESIAN_POINT('Ctrl Pts',(162.180163555531,2.19704526617383,339.400247170431));
#43795=CARTESIAN_POINT('Ctrl Pts',(162.172751751354,2.31373393254928,339.341984470144));
#43796=CARTESIAN_POINT('Ctrl Pts',(162.165339947177,2.42795595662479,339.279150622085));
#43797=CARTESIAN_POINT('Ctrl Pts',(162.157928143,2.53934448884438,339.211996276052));
#43798=CARTESIAN_POINT('Ctrl Pts',(162.150153064222,2.65619250483726,339.141550495477));
#43799=CARTESIAN_POINT('Ctrl Pts',(162.142377985443,2.77029151148098,339.066127365561));
#43800=CARTESIAN_POINT('Ctrl Pts',(162.134602906665,2.8811884478948,338.985967409578));
#43801=CARTESIAN_POINT('Ctrl Pts',(162.126837395616,2.99194891856831,338.905906095524));
#43802=CARTESIAN_POINT('Ctrl Pts',(162.119071884567,3.0995148454276,338.821119780165));
#43803=CARTESIAN_POINT('Ctrl Pts',(162.111306373518,3.20345893854672,338.731894142596));
#43804=CARTESIAN_POINT('Ctrl Pts',(162.103548561995,3.30729997079486,338.642756972507));
#43805=CARTESIAN_POINT('Ctrl Pts',(162.095790750473,3.40752602103372,338.549189492596));
#43806=CARTESIAN_POINT('Ctrl Pts',(162.088032938951,3.50374020827666,338.451519609593));
#43807=CARTESIAN_POINT('Ctrl Pts',(162.080280965428,3.59988199129257,338.353923226275));
#43808=CARTESIAN_POINT('Ctrl Pts',(162.072528991905,3.69201764738974,338.252230862099));
#43809=CARTESIAN_POINT('Ctrl Pts',(162.064777018382,3.77978500167942,338.146809241689));
#43810=CARTESIAN_POINT('Ctrl Pts',(162.057028327824,3.86751518644246,338.041432267397));
#43811=CARTESIAN_POINT('Ctrl Pts',(162.049279637267,3.95088049930486,337.932329477842));
#43812=CARTESIAN_POINT('Ctrl Pts',(162.041530946709,4.02955729213068,337.819902674196));
#43813=CARTESIAN_POINT('Ctrl Pts',(162.033783868331,4.10821771559263,337.707499261885));
#43814=CARTESIAN_POINT('Ctrl Pts',(162.026036789953,4.18219133535917,337.591773531149));
#43815=CARTESIAN_POINT('Ctrl Pts',(162.018289711576,4.25119654658299,337.473158099439));
#43816=CARTESIAN_POINT('Ctrl Pts',(162.01054256827,4.32020233613688,337.354541673618));
#43817=CARTESIAN_POINT('Ctrl Pts',(162.002795424964,4.38423943754145,337.233035836379));
#43818=CARTESIAN_POINT('Ctrl Pts',(161.995048281658,4.44307132122676,337.109099404246));
#43819=CARTESIAN_POINT('Ctrl Pts',(161.98729939663,4.50191643156854,336.985135108572));
#43820=CARTESIAN_POINT('Ctrl Pts',(161.979550511602,4.55555382795097,336.858739483672));
#43821=CARTESIAN_POINT('Ctrl Pts',(161.971801626574,4.60379456799849,336.730392625437));
#43822=CARTESIAN_POINT('Ctrl Pts',(161.964044516799,4.65208651126594,336.601909538521));
#43823=CARTESIAN_POINT('Ctrl Pts',(161.956287407024,4.6949702181088,336.471471447597));
#43824=CARTESIAN_POINT('Ctrl Pts',(161.94853029725,4.73230605133504,336.339575492086));
#43825=CARTESIAN_POINT('Ctrl Pts',(161.940769042323,4.76966183563678,336.207609055593));
#43826=CARTESIAN_POINT('Ctrl Pts',(161.933007787397,4.8014637484968,336.074183582244));
#43827=CARTESIAN_POINT('Ctrl Pts',(161.925246532471,4.82762324614092,335.939806818351));
#43828=CARTESIAN_POINT('Ctrl Pts',(161.917472862066,4.8538245904559,335.80521509543));
#43829=CARTESIAN_POINT('Ctrl Pts',(161.909699191662,4.87436542428713,335.669669427714));
#43830=CARTESIAN_POINT('Ctrl Pts',(161.901925521257,4.88920898072962,335.533683993814));
#43831=CARTESIAN_POINT('Ctrl Pts',(161.89451371708,4.90336156604838,335.404028714579));
#43832=CARTESIAN_POINT('Ctrl Pts',(161.887101912903,4.91233533399939,335.273973977125));
#43833=CARTESIAN_POINT('Ctrl Pts',(161.879690108726,4.91614253800159,335.143963914059));
#43834=CARTESIAN_POINT('Ctrl Pts',(161.871915029948,4.92013634441305,335.007581670521));
#43835=CARTESIAN_POINT('Ctrl Pts',(161.864139951169,4.91845694487922,334.870817598263));
#43836=CARTESIAN_POINT('Ctrl Pts',(161.856364872391,4.91106142331369,334.734182846791));
#43837=CARTESIAN_POINT('Ctrl Pts',(161.848599361342,4.90367500240827,334.597716233079));
#43838=CARTESIAN_POINT('Ctrl Pts',(161.840833850293,4.89058647614153,334.461379010087));
#43839=CARTESIAN_POINT('Ctrl Pts',(161.833068339244,4.87180484706228,334.325685092379));
#43840=CARTESIAN_POINT('Ctrl Pts',(161.825310527722,4.85304184002295,334.190125715585));
#43841=CARTESIAN_POINT('Ctrl Pts',(161.817552716199,4.82859701674449,334.055208759429));
#43842=CARTESIAN_POINT('Ctrl Pts',(161.809794904677,4.79853134591831,333.921445418748));
#43843=CARTESIAN_POINT('Ctrl Pts',(161.802042931154,4.76848830046288,333.787782739223));
#43844=CARTESIAN_POINT('Ctrl Pts',(161.794290957631,4.73283291217347,333.655272327021));
#43845=CARTESIAN_POINT('Ctrl Pts',(161.786538984108,4.69167757399479,333.524417198469));
#43846=CARTESIAN_POINT('Ctrl Pts',(161.778790293551,4.65053966512626,333.393617487142));
#43847=CARTESIAN_POINT('Ctrl Pts',(161.771041602993,4.60390655607368,333.26447203729));
#43848=CARTESIAN_POINT('Ctrl Pts',(161.763292912435,4.55194098543875,333.137470449205));
#43849=CARTESIAN_POINT('Ctrl Pts',(161.755545834057,4.49998622667481,333.010495284862));
#43850=CARTESIAN_POINT('Ctrl Pts',(161.74779875568,4.44270136105948,332.8856634566));
#43851=CARTESIAN_POINT('Ctrl Pts',(161.740051677302,4.38029779329731,332.763445886071));
#43852=CARTESIAN_POINT('Ctrl Pts',(161.732304533996,4.31789370253317,332.64122729124));
#43853=CARTESIAN_POINT('Ctrl Pts',(161.72455739069,4.25037100180412,332.521623345964));
#43854=CARTESIAN_POINT('Ctrl Pts',(161.716810247384,4.1779875199909,332.405081244952));
#43855=CARTESIAN_POINT('Ctrl Pts',(161.709061362356,4.10558776483425,332.288512942801));
#43856=CARTESIAN_POINT('Ctrl Pts',(161.701312477328,4.02832526021898,332.175008186667));
#43857=CARTESIAN_POINT('Ctrl Pts',(161.6935635923,3.94650148146258,332.064985669658));
#43858=CARTESIAN_POINT('Ctrl Pts',(161.685806482525,3.86459085410195,331.954846373613));
#43859=CARTESIAN_POINT('Ctrl Pts',(161.678049372751,3.77810951510899,331.84819701411));
#43860=CARTESIAN_POINT('Ctrl Pts',(161.670292262976,3.68739995393148,331.745424045709));
#43861=CARTESIAN_POINT('Ctrl Pts',(161.66253100805,3.59664192046482,331.642596158721));
#43862=CARTESIAN_POINT('Ctrl Pts',(161.654769753124,3.5016514332598,331.543649072151));
#43863=CARTESIAN_POINT('Ctrl Pts',(161.647008498198,3.40280755090739,331.448932015015));
#43864=CARTESIAN_POINT('Ctrl Pts',(161.639234827793,3.30380555055638,331.354063441455));
#43865=CARTESIAN_POINT('Ctrl Pts',(161.631461157388,3.20093813065343,331.263438677657));
#43866=CARTESIAN_POINT('Ctrl Pts',(161.623687486984,3.09461777827886,331.177366893245));
#43867=CARTESIAN_POINT('Ctrl Pts',(161.616275682806,2.99324666388503,331.095301771104));
#43868=CARTESIAN_POINT('Ctrl Pts',(161.608863878629,2.88873708131458,331.017375457209));
#43869=CARTESIAN_POINT('Ctrl Pts',(161.601452074452,2.78146914217968,330.943817993038));
#43870=CARTESIAN_POINT('Ctrl Pts',(161.593676995674,2.6689436818145,330.866655258432));
#43871=CARTESIAN_POINT('Ctrl Pts',(161.585901916895,2.55302703626747,330.794056614309));
#43872=CARTESIAN_POINT('Ctrl Pts',(161.578126838117,2.43412581770559,330.726334762048));
#43873=CARTESIAN_POINT('Ctrl Pts',(161.570361327068,2.31537091466275,330.658696245838));
#43874=CARTESIAN_POINT('Ctrl Pts',(161.562595816019,2.19363908263863,330.595922772417));
#43875=CARTESIAN_POINT('Ctrl Pts',(161.55483030497,2.0693673551506,330.538284880011));
#43876=CARTESIAN_POINT('Ctrl Pts',(161.547072493447,1.94521884344229,330.480704135743));
#43877=CARTESIAN_POINT('Ctrl Pts',(161.539314681925,1.81853580016415,330.428249002637));
#43878=CARTESIAN_POINT('Ctrl Pts',(161.531556870403,1.68978109361745,330.381144847676));
#43879=CARTESIAN_POINT('Ctrl Pts',(161.52380489688,1.56112327907038,330.334076140085));
#43880=CARTESIAN_POINT('Ctrl Pts',(161.516052923357,1.43039726995477,330.292350529284));
#43881=CARTESIAN_POINT('Ctrl Pts',(161.508300949834,1.29808688570233,330.256145712644));
#43882=CARTESIAN_POINT('Ctrl Pts',(161.500552259276,1.16583253497618,330.219956228765));
#43883=CARTESIAN_POINT('Ctrl Pts',(161.492803568719,1.03199551988241,330.189282991762));
#43884=CARTESIAN_POINT('Ctrl Pts',(161.485054878161,0.897075622947639,330.164254102084));
#43885=CARTESIAN_POINT('Ctrl Pts',(161.477307799783,0.762183797224345,330.139230419875));
#43886=CARTESIAN_POINT('Ctrl Pts',(161.469560721405,0.626209921878928,330.119848820369));
#43887=CARTESIAN_POINT('Ctrl Pts',(161.461813643028,0.489664408190774,330.106186371566));
#43888=CARTESIAN_POINT('Ctrl Pts',(161.454066499722,0.353117750119721,330.092523808258));
#43889=CARTESIAN_POINT('Ctrl Pts',(161.446319356416,0.215999833082388,330.084580530173));
#43890=CARTESIAN_POINT('Ctrl Pts',(161.43857221311,0.078826238651887,330.082381726222));
#43891=CARTESIAN_POINT('Ctrl Pts',(161.430823328082,-0.0583781953148501,
330.080182427932));
#43892=CARTESIAN_POINT('Ctrl Pts',(161.423074443054,-0.19563794083539,330.083730179941));
#43893=CARTESIAN_POINT('Ctrl Pts',(161.415325558026,-0.332437764348275,
330.092998044087));
#43894=CARTESIAN_POINT('Ctrl Pts',(161.407568448251,-0.46938278860729,330.10227574524));
#43895=CARTESIAN_POINT('Ctrl Pts',(161.399811338476,-0.605866525105003,
330.117285660232));
#43896=CARTESIAN_POINT('Ctrl Pts',(161.392054228702,-0.7413786552649,330.137948915116));
#43897=CARTESIAN_POINT('Ctrl Pts',(161.384292973775,-0.876963198774339,
330.158623211784));
#43898=CARTESIAN_POINT('Ctrl Pts',(161.376531718849,-1.01157471799402,330.184956792883));
#43899=CARTESIAN_POINT('Ctrl Pts',(161.368770463923,-1.14471440844185,330.216819887815));
#43900=CARTESIAN_POINT('Ctrl Pts',(161.360996793518,-1.27806707900423,330.248733953314));
#43901=CARTESIAN_POINT('Ctrl Pts',(161.353223123114,-1.40994283971743,330.286195101552));
#43902=CARTESIAN_POINT('Ctrl Pts',(161.345449452709,-1.53985848282114,330.329023772766));
#43903=CARTESIAN_POINT('Ctrl Pts',(161.338037648532,-1.66372652148162,330.369858759031));
#43904=CARTESIAN_POINT('Ctrl Pts',(161.330625844355,-1.78581255320543,330.415572696768));
#43905=CARTESIAN_POINT('Ctrl Pts',(161.323214040178,-1.90571743100325,330.465970430658));
#43906=CARTESIAN_POINT('Ctrl Pts',(161.3154389614,-2.03149920404092,330.518838307612));
#43907=CARTESIAN_POINT('Ctrl Pts',(161.307663882621,-2.15527810090941,330.577027795782));
#43908=CARTESIAN_POINT('Ctrl Pts',(161.299888803843,-2.27657112317238,330.640366186979));
#43909=CARTESIAN_POINT('Ctrl Pts',(161.292123292794,-2.3977148866496,330.703626636253));
#43910=CARTESIAN_POINT('Ctrl Pts',(161.284357781745,-2.51637851894135,330.772023202428));
#43911=CARTESIAN_POINT('Ctrl Pts',(161.276592270696,-2.63209801476996,330.845334778452));
#43912=CARTESIAN_POINT('Ctrl Pts',(161.268834459174,-2.74770277438154,330.918573665834));
#43913=CARTESIAN_POINT('Ctrl Pts',(161.261076647651,-2.86036887868161,330.996717657191));
#43914=CARTESIAN_POINT('Ctrl Pts',(161.253318836129,-2.96965632716724,331.079499475703));
#43915=CARTESIAN_POINT('Ctrl Pts',(161.245566862606,-3.07886153338226,331.16221899827));
#43916=CARTESIAN_POINT('Ctrl Pts',(161.237814889083,-3.18469283427131,331.249569166033));
#43917=CARTESIAN_POINT('Ctrl Pts',(161.23006291556,-3.28673897786701,331.341239287153));
#43918=CARTESIAN_POINT('Ctrl Pts',(161.222314225003,-3.38874190486018,331.432870585923));
#43919=CARTESIAN_POINT('Ctrl Pts',(161.214565534445,-3.48696257267444,331.52881793863));
#43920=CARTESIAN_POINT('Ctrl Pts',(161.206816843887,-3.58102279790618,331.62873038999));
#43921=CARTESIAN_POINT('Ctrl Pts',(161.19906976551,-3.6750634531224,331.72862205373));
#43922=CARTESIAN_POINT('Ctrl Pts',(161.191322687132,-3.76494511976427,331.832476890774));
#43923=CARTESIAN_POINT('Ctrl Pts',(161.183575608754,-3.85032677687502,331.939907391307));
#43924=CARTESIAN_POINT('Ctrl Pts',(161.175828465448,-3.93570914956624,332.04733879221));
#43925=CARTESIAN_POINT('Ctrl Pts',(161.168081322142,-4.01659119430352,332.158345610372));
#43926=CARTESIAN_POINT('Ctrl Pts',(161.160334178837,-4.09267271842105,332.272507913414));
#43927=CARTESIAN_POINT('Ctrl Pts',(161.152585293808,-4.16877134728048,332.386695882564));
#43928=CARTESIAN_POINT('Ctrl Pts',(161.14483640878,-4.24006709119236,332.504040423062));
#43929=CARTESIAN_POINT('Ctrl Pts',(161.137087523752,-4.30630378058577,332.62409368623));
#43930=CARTESIAN_POINT('Ctrl Pts',(161.129330413978,-4.37261077428567,332.744274375171));
#43931=CARTESIAN_POINT('Ctrl Pts',(161.121573304203,-4.43384779780058,332.867169187216));
#43932=CARTESIAN_POINT('Ctrl Pts',(161.113816194428,-4.48980501525064,332.992306301367));
#43933=CARTESIAN_POINT('Ctrl Pts',(161.106054939502,-4.54579213444854,333.117510284791));
#43934=CARTESIAN_POINT('Ctrl Pts',(161.098293684576,-4.59649368135744,333.244958594867));
#43935=CARTESIAN_POINT('Ctrl Pts',(161.09053242965,-4.64174885111503,333.374161549947));
#43936=CARTESIAN_POINT('Ctrl Pts',(161.082758759245,-4.6870764143956,333.503571187647));
#43937=CARTESIAN_POINT('Ctrl Pts',(161.07498508884,-4.72694007679532,333.634740705109));
#43938=CARTESIAN_POINT('Ctrl Pts',(161.067211418436,-4.76122934250337,333.767166592526));
#43939=CARTESIAN_POINT('Ctrl Pts',(161.059799614259,-4.79392243464328,333.893428023024));
#43940=CARTESIAN_POINT('Ctrl Pts',(161.052387810082,-4.82154836619667,334.020831206468));
#43941=CARTESIAN_POINT('Ctrl Pts',(161.044976005905,-4.84405524609774,334.148934881896));
#43942=CARTESIAN_POINT('Ctrl Pts',(161.032948588466,-4.88057801887158,334.356813603857));
#43943=CARTESIAN_POINT('Ctrl Pts',(161.020921171028,-4.90372683021974,334.567106545968));
#43944=CARTESIAN_POINT('Ctrl Pts',(161.00889375359,-4.91325675924559,334.778434930037));
#43945=CARTESIAN_POINT('Ctrl Pts',(161.004774585223,-4.91652058395112,334.850810999055));
#43946=CARTESIAN_POINT('Ctrl Pts',(161.000655416857,-4.91818733857957,334.923308266447));
#43947=CARTESIAN_POINT('Ctrl Pts',(160.99653624849,-4.91824826623568,334.995870330555));
#43948=CARTESIAN_POINT('',(164.496536248442,-4.91824939077852,335.002447980137));
#43949=CARTESIAN_POINT('Ctrl Pts',(164.496536248442,-4.91824939077852,335.002447980137));
#43950=CARTESIAN_POINT('Ctrl Pts',(164.48801435836,-4.91817413949945,335.15363570911));
#43951=CARTESIAN_POINT('Ctrl Pts',(164.479492468279,-4.91112349237319,335.304585905361));
#43952=CARTESIAN_POINT('Ctrl Pts',(164.470970578197,-4.89718756698481,335.454683402237));
#43953=CARTESIAN_POINT('Ctrl Pts',(164.462404819792,-4.88317990332284,335.60555355934));
#43954=CARTESIAN_POINT('Ctrl Pts',(164.453839061386,-4.86221597859101,335.755561974361));
#43955=CARTESIAN_POINT('Ctrl Pts',(164.445273302981,-4.83443761129456,335.904099576928));
#43956=CARTESIAN_POINT('Ctrl Pts',(164.436684914085,-4.80658585433951,336.053029611628));
#43957=CARTESIAN_POINT('Ctrl Pts',(164.428096525189,-4.77188371897625,336.200480825931));
#43958=CARTESIAN_POINT('Ctrl Pts',(164.419508136293,-4.73052300940142,336.345858506688));
#43959=CARTESIAN_POINT('Ctrl Pts',(164.410889304865,-4.68901569203211,336.491751495363));
#43960=CARTESIAN_POINT('Ctrl Pts',(164.402270473436,-4.64080263496645,336.635556003889));
#43961=CARTESIAN_POINT('Ctrl Pts',(164.393651642007,-4.5861250243414,336.776693649341));
#43962=CARTESIAN_POINT('Ctrl Pts',(164.390378567069,-4.56536073413448,336.830291877131));
#43963=CARTESIAN_POINT('Ctrl Pts',(164.38710549213,-4.54366462411572,336.883505748913));
#43964=CARTESIAN_POINT('Ctrl Pts',(164.383832417192,-4.52105162432562,336.936304540273));
#43965=CARTESIAN_POINT('Ctrl Pts',(164.376057338413,-4.46733520838884,337.061726282811));
#43966=CARTESIAN_POINT('Ctrl Pts',(164.368282259635,-4.40831083353155,337.185109243612));
#43967=CARTESIAN_POINT('Ctrl Pts',(164.360507180857,-4.34415446699743,337.305971602029));
#43968=CARTESIAN_POINT('Ctrl Pts',(164.352741669808,-4.2800770489568,337.42668523162));
#43969=CARTESIAN_POINT('Ctrl Pts',(164.344976158758,-4.21088038627454,337.544884088496));
#43970=CARTESIAN_POINT('Ctrl Pts',(164.337210647709,-4.13678871564286,337.660105671704));
#43971=CARTESIAN_POINT('Ctrl Pts',(164.329452836187,-4.06277050711833,337.775213012376));
#43972=CARTESIAN_POINT('Ctrl Pts',(164.321695024665,-3.98386715926199,337.887348627327));
#43973=CARTESIAN_POINT('Ctrl Pts',(164.313937213143,-3.90034891531345,337.99607433174));
#43974=CARTESIAN_POINT('Ctrl Pts',(164.30618523962,-3.81689352149178,338.104718216614));
#43975=CARTESIAN_POINT('Ctrl Pts',(164.298433266097,-3.72883038127933,338.209956989849));
#43976=CARTESIAN_POINT('Ctrl Pts',(164.290681292574,-3.63647295772348,338.311381507807));
#43977=CARTESIAN_POINT('Ctrl Pts',(164.282932602016,-3.54415464759149,338.412763072422));
#43978=CARTESIAN_POINT('Ctrl Pts',(164.275183911459,-3.44754593386803,338.510333306152));
#43979=CARTESIAN_POINT('Ctrl Pts',(164.267435220901,-3.34700031872777,338.603716405176));
#43980=CARTESIAN_POINT('Ctrl Pts',(164.259688142523,-3.24647562294249,338.697080075067));
#43981=CARTESIAN_POINT('Ctrl Pts',(164.251941064145,-3.14201594122153,338.786258077235));
#43982=CARTESIAN_POINT('Ctrl Pts',(164.244193985768,-3.03401107837778,338.870912016409));
#43983=CARTESIAN_POINT('Ctrl Pts',(164.236446842462,-2.92600531034933,338.955566665065));
#43984=CARTESIAN_POINT('Ctrl Pts',(164.228699699156,-2.8144546095731,339.035696933976));
#43985=CARTESIAN_POINT('Ctrl Pts',(164.22095255585,-2.69978092686067,339.111005474268));
#43986=CARTESIAN_POINT('Ctrl Pts',(164.213203670822,-2.5850814630697,339.186330945519));
#43987=CARTESIAN_POINT('Ctrl Pts',(164.205454785794,-2.46725794687209,339.256832316537));
#43988=CARTESIAN_POINT('Ctrl Pts',(164.197705900766,-2.34675994733358,339.322256449135));
#43989=CARTESIAN_POINT('Ctrl Pts',(164.189948790991,-2.22613404997346,339.387750023583));
#43990=CARTESIAN_POINT('Ctrl Pts',(164.182191681216,-2.10282834270516,339.44815540771));
#43991=CARTESIAN_POINT('Ctrl Pts',(164.174434571442,-1.9773160533486,339.50326595791));
#43992=CARTESIAN_POINT('Ctrl Pts',(164.166673316516,-1.85173669423774,339.558405957426));
#43993=CARTESIAN_POINT('Ctrl Pts',(164.158912061589,-1.72394876749512,339.608245343245));
#43994=CARTESIAN_POINT('Ctrl Pts',(164.151150806663,-1.59444302994478,339.652626622324));
#43995=CARTESIAN_POINT('Ctrl Pts',(164.143377136259,-1.46473012542015,339.697078896986));
#43996=CARTESIAN_POINT('Ctrl Pts',(164.135603465854,-1.33329429383625,339.736055506212));
#43997=CARTESIAN_POINT('Ctrl Pts',(164.127829795449,-1.2006397799857,339.769449358282));
#43998=CARTESIAN_POINT('Ctrl Pts',(164.120417991272,-1.07416036566921,339.801288718504));
#43999=CARTESIAN_POINT('Ctrl Pts',(164.113006187095,-0.946573456739391,
339.828053320418));
#44000=CARTESIAN_POINT('Ctrl Pts',(164.105594382918,-0.818320654648899,
339.849694255175));
#44001=CARTESIAN_POINT('Ctrl Pts',(164.09781930414,-0.683781800682978,339.872395876609));
#44002=CARTESIAN_POINT('Ctrl Pts',(164.090044225361,-0.548084960631892,
339.889530620364));
#44003=CARTESIAN_POINT('Ctrl Pts',(164.082269146583,-0.411730533729872,
339.90098572025));
#44004=CARTESIAN_POINT('Ctrl Pts',(164.074503635534,-0.275543899630949,
339.912426723906));
#44005=CARTESIAN_POINT('Ctrl Pts',(164.066738124485,-0.13870167454075,339.918201957715));
#44006=CARTESIAN_POINT('Ctrl Pts',(164.058972613436,-0.00171413271892654,
339.918249701291));
#44007=CARTESIAN_POINT('Ctrl Pts',(164.051214801913,0.135137585556445,339.918297397529));
#44008=CARTESIAN_POINT('Ctrl Pts',(164.043456990391,0.272133945475837,339.912628904578));
#44009=CARTESIAN_POINT('Ctrl Pts',(164.035699178869,0.408760223954992,339.901234348795));
#44010=CARTESIAN_POINT('Ctrl Pts',(164.027947205346,0.545283686826738,339.889848367778));
#44011=CARTESIAN_POINT('Ctrl Pts',(164.020195231823,0.681437234641364,339.872744933225));
#44012=CARTESIAN_POINT('Ctrl Pts',(164.0124432583,0.81670717694351,339.849966231803));
#44013=CARTESIAN_POINT('Ctrl Pts',(164.004694567742,0.951919832344895,339.827197177174));
#44014=CARTESIAN_POINT('Ctrl Pts',(163.996945877185,1.08624924186076,339.798757700798));
#44015=CARTESIAN_POINT('Ctrl Pts',(163.989197186627,1.21918808373027,339.764741701183));
#44016=CARTESIAN_POINT('Ctrl Pts',(163.981450108249,1.3520992665634,339.730732778881));
#44017=CARTESIAN_POINT('Ctrl Pts',(163.973703029872,1.48362007878995,339.691149737978));
#44018=CARTESIAN_POINT('Ctrl Pts',(163.965955951494,1.61325501085684,339.646137248559));
#44019=CARTESIAN_POINT('Ctrl Pts',(163.958208808188,1.74289102938928,339.601124381892));
#44020=CARTESIAN_POINT('Ctrl Pts',(163.950461664882,1.87064076698849,339.550682104161));
#44021=CARTESIAN_POINT('Ctrl Pts',(163.942714521576,1.99602583484769,339.495004330267));
#44022=CARTESIAN_POINT('Ctrl Pts',(163.934965636548,2.12143909193207,339.439314038828));
#44023=CARTESIAN_POINT('Ctrl Pts',(163.92721675152,2.24448626422885,339.378386067629));
#44024=CARTESIAN_POINT('Ctrl Pts',(163.919467866492,2.36471119481717,339.31246148129));
#44025=CARTESIAN_POINT('Ctrl Pts',(163.911710756717,2.48506373338902,339.246466921913));
#44026=CARTESIAN_POINT('Ctrl Pts',(163.903953646942,2.60258770307625,339.17546534147));
#44027=CARTESIAN_POINT('Ctrl Pts',(163.896196537168,2.71685324213598,339.099742860619));
#44028=CARTESIAN_POINT('Ctrl Pts',(163.888435282242,2.83117984104629,339.023979916095));
#44029=CARTESIAN_POINT('Ctrl Pts',(163.880674027315,2.94224422348891,338.943491273711));
#44030=CARTESIAN_POINT('Ctrl Pts',(163.872912772389,3.04964837352559,338.858604392828));
#44031=CARTESIAN_POINT('Ctrl Pts',(163.865139101985,3.15722433519939,338.7735817206));
#44032=CARTESIAN_POINT('Ctrl Pts',(163.85736543158,3.26112806768403,338.684147005491));
#44033=CARTESIAN_POINT('Ctrl Pts',(163.849591761175,3.36099663947487,338.590666324227));
#44034=CARTESIAN_POINT('Ctrl Pts',(163.842179956998,3.45621630522143,338.501537191167));
#44035=CARTESIAN_POINT('Ctrl Pts',(163.834768152821,3.54776782732529,338.40873049935));
#44036=CARTESIAN_POINT('Ctrl Pts',(163.827356348644,3.63537110140622,338.312591133472));
#44037=CARTESIAN_POINT('Ctrl Pts',(163.819581269866,3.72726807290682,338.211739690889));
#44038=CARTESIAN_POINT('Ctrl Pts',(163.811806191087,3.81511039091875,338.106901916162));
#44039=CARTESIAN_POINT('Ctrl Pts',(163.804031112309,3.89853243320858,337.998437581428));
#44040=CARTESIAN_POINT('Ctrl Pts',(163.79626560126,3.98185181936449,337.890106718963));
#44041=CARTESIAN_POINT('Ctrl Pts',(163.788500090211,4.06076151668513,337.778158482881));
#44042=CARTESIAN_POINT('Ctrl Pts',(163.780734579162,4.13493348449984,337.66298857325));
#44043=CARTESIAN_POINT('Ctrl Pts',(163.77297676764,4.20903191059251,337.547932854921));
#44044=CARTESIAN_POINT('Ctrl Pts',(163.765218956117,4.27840174513961,337.429662146381));
#44045=CARTESIAN_POINT('Ctrl Pts',(163.757461144595,4.34275613898933,337.308603946061));
#44046=CARTESIAN_POINT('Ctrl Pts',(163.749709171072,4.40706210411684,337.187636845876));
#44047=CARTESIAN_POINT('Ctrl Pts',(163.741957197549,4.46635995832735,337.063886772979));
#44048=CARTESIAN_POINT('Ctrl Pts',(163.734205224026,4.52040718990632,336.937808530259));
#44049=CARTESIAN_POINT('Ctrl Pts',(163.726456533469,4.57443153245066,336.811783681749));
#44050=CARTESIAN_POINT('Ctrl Pts',(163.718707842911,4.62320952134495,336.68343298297));
#44051=CARTESIAN_POINT('Ctrl Pts',(163.710959152353,4.66654557693405,336.553233865488));
#44052=CARTESIAN_POINT('Ctrl Pts',(163.703212073975,4.70987261609483,336.423061837018));
#44053=CARTESIAN_POINT('Ctrl Pts',(163.695464995598,4.74775985069061,336.291042525437));
#44054=CARTESIAN_POINT('Ctrl Pts',(163.68771791722,4.78006078823127,336.157670904581));
#44055=CARTESIAN_POINT('Ctrl Pts',(163.679970773914,4.81236199648488,336.024298165943));
#44056=CARTESIAN_POINT('Ctrl Pts',(163.672223630608,4.83907672229522,335.889573475317));
#44057=CARTESIAN_POINT('Ctrl Pts',(163.664476487302,4.86010914920729,335.754004058538));
#44058=CARTESIAN_POINT('Ctrl Pts',(163.656727602274,4.88114630465544,335.618404162875));
#44059=CARTESIAN_POINT('Ctrl Pts',(163.648978717246,4.89649855920798,335.481959549333));
#44060=CARTESIAN_POINT('Ctrl Pts',(163.641229832218,4.90612177656237,335.345184263895));
#44061=CARTESIAN_POINT('Ctrl Pts',(163.633472722443,4.91575520809909,335.208263803755));
#44062=CARTESIAN_POINT('Ctrl Pts',(163.625715612669,4.91964742787418,335.071012361134));
#44063=CARTESIAN_POINT('Ctrl Pts',(163.617958502894,4.91780641799855,334.933946252247));
#44064=CARTESIAN_POINT('Ctrl Pts',(163.610197247968,4.91596442434611,334.796806899614));
#44065=CARTESIAN_POINT('Ctrl Pts',(163.602435993042,4.90838311802871,334.659853468132));
#44066=CARTESIAN_POINT('Ctrl Pts',(163.594674738115,4.89512247734571,334.523597864945));
#44067=CARTESIAN_POINT('Ctrl Pts',(163.586901067711,4.88184062395925,334.387124297199));
#44068=CARTESIAN_POINT('Ctrl Pts',(163.579127397306,4.86286133566008,334.251351175755));
#44069=CARTESIAN_POINT('Ctrl Pts',(163.571353726902,4.8382960511165,334.116781802582));
#44070=CARTESIAN_POINT('Ctrl Pts',(163.563941922724,4.81487428647819,333.988476666104));
#44071=CARTESIAN_POINT('Ctrl Pts',(163.556530118547,4.7863749412202,333.861266011809));
#44072=CARTESIAN_POINT('Ctrl Pts',(163.54911831437,4.75293645569013,333.735572022347));
#44073=CARTESIAN_POINT('Ctrl Pts',(163.541343235592,4.71785905037651,333.603717396039));
#44074=CARTESIAN_POINT('Ctrl Pts',(163.533568156813,4.67723524766031,333.473115181295));
#44075=CARTESIAN_POINT('Ctrl Pts',(163.525793078035,4.63116972843598,333.344267530995));
#44076=CARTESIAN_POINT('Ctrl Pts',(163.518027566986,4.58516089576573,333.215578435931));
#44077=CARTESIAN_POINT('Ctrl Pts',(163.510262055937,4.53372380079088,333.088639973857));
#44078=CARTESIAN_POINT('Ctrl Pts',(163.502496544888,4.47701367451134,332.963942137183));
#44079=CARTESIAN_POINT('Ctrl Pts',(163.494738733365,4.42035977648714,332.839367938777));
#44080=CARTESIAN_POINT('Ctrl Pts',(163.486980921843,4.35844341239523,332.717030298203));
#44081=CARTESIAN_POINT('Ctrl Pts',(163.479223110321,4.291468844249,332.597401776963));
#44082=CARTESIAN_POINT('Ctrl Pts',(163.471471136798,4.22454467658916,332.477863279979));
#44083=CARTESIAN_POINT('Ctrl Pts',(163.463719163275,4.15257007162135,332.361030184086));
#44084=CARTESIAN_POINT('Ctrl Pts',(163.455967189752,4.07579624579284,332.2473525425));
#44085=CARTESIAN_POINT('Ctrl Pts',(163.448218499194,3.99905493372514,332.133723043462));
#44086=CARTESIAN_POINT('Ctrl Pts',(163.440469808637,3.91751866155143,332.023246664098));
#44087=CARTESIAN_POINT('Ctrl Pts',(163.432721118079,3.83148307228506,331.916346237125));
#44088=CARTESIAN_POINT('Ctrl Pts',(163.424974039701,3.74546538344163,331.809468051679));
#44089=CARTESIAN_POINT('Ctrl Pts',(163.417226961323,3.65495048443267,331.706164643055));
#44090=CARTESIAN_POINT('Ctrl Pts',(163.409479882946,3.56027533382699,331.60682705866));
#44091=CARTESIAN_POINT('Ctrl Pts',(163.40173273964,3.4655993897524,331.50748864172));
#44092=CARTESIAN_POINT('Ctrl Pts',(163.393985596334,3.36676339420635,331.412116398254));
#44093=CARTESIAN_POINT('Ctrl Pts',(163.386238453028,3.26414203243208,331.321065391365));
#44094=CARTESIAN_POINT('Ctrl Pts',(163.378489568,3.16149759919699,331.229993914278));
#44095=CARTESIAN_POINT('Ctrl Pts',(163.370740682972,3.05506639860117,331.14324586632));
#44096=CARTESIAN_POINT('Ctrl Pts',(163.362991797944,2.94525681819376,331.06113654243));
#44097=CARTESIAN_POINT('Ctrl Pts',(163.355234688169,2.83533068476313,330.978940066854));
#44098=CARTESIAN_POINT('Ctrl Pts',(163.347477578394,2.72201932198736,330.90139238512));
#44099=CARTESIAN_POINT('Ctrl Pts',(163.33972046862,2.60576123076575,330.82876619323));
#44100=CARTESIAN_POINT('Ctrl Pts',(163.331959213693,2.48944101493743,330.756101192226));
#44101=CARTESIAN_POINT('Ctrl Pts',(163.324197958767,2.37017127276737,330.688363114287));
#44102=CARTESIAN_POINT('Ctrl Pts',(163.316436703841,2.24841493559251,330.625778544712));
#44103=CARTESIAN_POINT('Ctrl Pts',(163.308663033436,2.12646382795849,330.563093860221));
#44104=CARTESIAN_POINT('Ctrl Pts',(163.300889363032,2.00201853161359,330.505579321984));
#44105=CARTESIAN_POINT('Ctrl Pts',(163.293115692627,1.87556258977798,330.453413584421));
#44106=CARTESIAN_POINT('Ctrl Pts',(163.28570388845,1.75499320245967,330.403676174493));
#44107=CARTESIAN_POINT('Ctrl Pts',(163.278292084273,1.63259641833461,330.358800897544));
#44108=CARTESIAN_POINT('Ctrl Pts',(163.270880280096,1.50880217781459,330.318899803388));
#44109=CARTESIAN_POINT('Ctrl Pts',(163.263105201318,1.37894041280134,330.277043037748));
#44110=CARTESIAN_POINT('Ctrl Pts',(163.255330122539,1.24713035350329,330.240528107771));
#44111=CARTESIAN_POINT('Ctrl Pts',(163.247555043761,1.11385091983099,330.209538728797));
#44112=CARTESIAN_POINT('Ctrl Pts',(163.239789532712,0.98073549498679,330.178587484228));
#44113=CARTESIAN_POINT('Ctrl Pts',(163.232024021663,0.84615467056458,330.153148349199));
#44114=CARTESIAN_POINT('Ctrl Pts',(163.224258510614,0.710604496037439,330.13335594966));
#44115=CARTESIAN_POINT('Ctrl Pts',(163.216500699092,0.575188719903009,330.113583174343));
#44116=CARTESIAN_POINT('Ctrl Pts',(163.208742887569,0.438805890615215,330.099446048789));
#44117=CARTESIAN_POINT('Ctrl Pts',(163.200985076047,0.301963933117836,330.091028534856));
#44118=CARTESIAN_POINT('Ctrl Pts',(163.193233102524,0.165224953533006,330.08261735537));
#44119=CARTESIAN_POINT('Ctrl Pts',(163.185481129001,0.0280279220224473,
330.079917244129));
#44120=CARTESIAN_POINT('Ctrl Pts',(163.177729155478,-0.109112754430488,
330.082960497482));
#44121=CARTESIAN_POINT('Ctrl Pts',(163.169980464921,-0.246195351725502,
330.086002462015));
#44122=CARTESIAN_POINT('Ctrl Pts',(163.162231774363,-0.383221251466671,
330.094782944779));
#44123=CARTESIAN_POINT('Ctrl Pts',(163.154483083805,-0.519674895201839,
330.109282152301));
#44124=CARTESIAN_POINT('Ctrl Pts',(163.146736005428,-0.656100148616698,
330.123778343143));
#44125=CARTESIAN_POINT('Ctrl Pts',(163.13898892705,-0.791952994407409,330.143990850815));
#44126=CARTESIAN_POINT('Ctrl Pts',(163.131241848672,-0.926722244851329,
330.16984793786));
#44127=CARTESIAN_POINT('Ctrl Pts',(163.123494705366,-1.06149262479126,330.195705241611));
#44128=CARTESIAN_POINT('Ctrl Pts',(163.11574756206,-1.19517900739775,330.227207145442));
#44129=CARTESIAN_POINT('Ctrl Pts',(163.108000418755,-1.32728004884665,330.264230713555));
#44130=CARTESIAN_POINT('Ctrl Pts',(163.100251533726,-1.45941078941435,330.301262605353));
#44131=CARTESIAN_POINT('Ctrl Pts',(163.092502648698,-1.58995510329353,330.343818526192));
#44132=CARTESIAN_POINT('Ctrl Pts',(163.08475376367,-1.71842685030941,330.391725678452));
#44133=CARTESIAN_POINT('Ctrl Pts',(163.076996653896,-1.84703495856495,330.439683679859));
#44134=CARTESIAN_POINT('Ctrl Pts',(163.069239544121,-1.97356573874499,330.493004121937));
#44135=CARTESIAN_POINT('Ctrl Pts',(163.061482434346,-2.09755257696487,330.551465831381));
#44136=CARTESIAN_POINT('Ctrl Pts',(163.05372117942,-2.22160566978676,330.609958780894));
#44137=CARTESIAN_POINT('Ctrl Pts',(163.045959924494,-2.34311176583828,330.67359829081));
#44138=CARTESIAN_POINT('Ctrl Pts',(163.038198669568,-2.46162980599996,330.742117690599));
#44139=CARTESIAN_POINT('Ctrl Pts',(163.030424999163,-2.58033743640092,330.810746699097));
#44140=CARTESIAN_POINT('Ctrl Pts',(163.022651328758,-2.69604712914511,330.884270986893));
#44141=CARTESIAN_POINT('Ctrl Pts',(163.014877658354,-2.80834697693655,330.962380612337));
#44142=CARTESIAN_POINT('Ctrl Pts',(163.007465854177,-2.91541923979571,331.036854215925));
#44143=CARTESIAN_POINT('Ctrl Pts',(163.000054049999,-3.01939174057162,331.115495695617));
#44144=CARTESIAN_POINT('Ctrl Pts',(162.992642245822,-3.11993758875825,331.198004141934));
#44145=CARTESIAN_POINT('Ctrl Pts',(162.984971950382,-3.22399003570806,331.283390121446));
#44146=CARTESIAN_POINT('Ctrl Pts',(162.977301654941,-3.32472052302233,331.373203600424));
#44147=CARTESIAN_POINT('Ctrl Pts',(162.9696313595,-3.42172113219513,331.467153052284));
#44148=CARTESIAN_POINT('Ctrl Pts',(162.961970553342,-3.51860173735074,331.560986274856));
#44149=CARTESIAN_POINT('Ctrl Pts',(162.954309747185,-3.61176135496804,331.658945017541));
#44150=CARTESIAN_POINT('Ctrl Pts',(162.946648941027,-3.70082357338688,331.760696380213));
#44151=CARTESIAN_POINT('Ctrl Pts',(162.938995661286,-3.78979829196516,331.862347776501));
#44152=CARTESIAN_POINT('Ctrl Pts',(162.931342381545,-3.87468335526745,331.967784080454));
#44153=CARTESIAN_POINT('Ctrl Pts',(162.923689101803,-3.95513818248469,332.076634641385));
#44154=CARTESIAN_POINT('Ctrl Pts',(162.9160414755,-4.03553357814199,332.185404794976));
#44155=CARTESIAN_POINT('Ctrl Pts',(162.908393849196,-4.11150501114932,332.297583864859));
#44156=CARTESIAN_POINT('Ctrl Pts',(162.900746222892,-4.18275163918189,332.412767542832));
#44157=CARTESIAN_POINT('Ctrl Pts',(162.89310159564,-4.25397032752569,332.527906051004));
#44158=CARTESIAN_POINT('Ctrl Pts',(162.885456968388,-4.32046768349657,332.646046483016));
#44159=CARTESIAN_POINT('Ctrl Pts',(162.877812341136,-4.38198595454,332.766755240303));
#44160=CARTESIAN_POINT('Ctrl Pts',(162.870168952057,-4.44349426168674,332.887444446819));
#44161=CARTESIAN_POINT('Ctrl Pts',(162.862525562978,-4.50002490540647,333.010700792823));
#44162=CARTESIAN_POINT('Ctrl Pts',(162.854882173899,-4.55136617113473,333.136066246148));
#44163=CARTESIAN_POINT('Ctrl Pts',(162.847238263366,-4.60271093950638,333.261440252251));
#44164=CARTESIAN_POINT('Ctrl Pts',(162.839594352834,-4.64886547449734,333.388923279055));
#44165=CARTESIAN_POINT('Ctrl Pts',(162.831950442302,-4.68966648554024,333.518038017728));
#44166=CARTESIAN_POINT('Ctrl Pts',(162.824300353631,-4.73050047372324,333.647257112511));
#44167=CARTESIAN_POINT('Ctrl Pts',(162.81665026496,-4.76597217494867,333.7781101689));
#44168=CARTESIAN_POINT('Ctrl Pts',(162.809000176289,-4.79596835592378,333.910105238347));
#44169=CARTESIAN_POINT('Ctrl Pts',(162.801346840274,-4.82597726981325,334.042156337658));
#44170=CARTESIAN_POINT('Ctrl Pts',(162.793693504259,-4.85050596118483,334.175350020076));
#44171=CARTESIAN_POINT('Ctrl Pts',(162.786040168244,-4.86949271350167,334.309186149781));
#44172=CARTESIAN_POINT('Ctrl Pts',(162.778376692472,-4.88850462099753,334.443199596372));
#44173=CARTESIAN_POINT('Ctrl Pts',(162.770713216701,-4.90195988485668,334.577856790165));
#44174=CARTESIAN_POINT('Ctrl Pts',(162.76304974093,-4.90984881383883,334.712654062591));
#44175=CARTESIAN_POINT('Ctrl Pts',(162.757545243462,-4.91551524913529,334.809475826872));
#44176=CARTESIAN_POINT('Ctrl Pts',(162.752040745995,-4.91831098889184,334.906369812791));
#44177=CARTESIAN_POINT('Ctrl Pts',(162.746536248527,-4.91824899084518,335.003150642852));
#44178=CARTESIAN_POINT('',(166.246536248533,-4.9182482206735,334.995816419961));
#44179=CARTESIAN_POINT('Ctrl Pts',(166.24653624849,-4.91824822067415,334.995816420722));
#44180=CARTESIAN_POINT('Ctrl Pts',(166.238483097421,-4.9183694473876,335.138331484532));
#44181=CARTESIAN_POINT('Ctrl Pts',(166.230429946352,-4.91229114364639,335.280950775894));
#44182=CARTESIAN_POINT('Ctrl Pts',(166.222376795283,-4.90001804275799,335.423091294103));
#44183=CARTESIAN_POINT('Ctrl Pts',(166.214669495024,-4.88827202274059,335.559127442372));
#44184=CARTESIAN_POINT('Ctrl Pts',(166.206962194764,-4.87085227486632,335.694724653029));
#44185=CARTESIAN_POINT('Ctrl Pts',(166.199254894505,-4.84781615683562,335.829374205063));
#44186=CARTESIAN_POINT('Ctrl Pts',(166.191548140149,-4.82478167043767,335.964014219959));
#44187=CARTESIAN_POINT('Ctrl Pts',(166.183841385792,-4.79613167145662,336.097706320243));
#44188=CARTESIAN_POINT('Ctrl Pts',(166.176134631436,-4.76197497548818,336.229950159691));
#44189=CARTESIAN_POINT('Ctrl Pts',(166.168426712617,-4.72781311856482,336.362213980711));
#44190=CARTESIAN_POINT('Ctrl Pts',(166.160718793797,-4.68814300815376,336.493028722961));
#44191=CARTESIAN_POINT('Ctrl Pts',(166.153010874978,-4.64312372530918,336.621907868521));
#44192=CARTESIAN_POINT('Ctrl Pts',(166.145300080857,-4.5980876488272,336.750835090139));
#44193=CARTESIAN_POINT('Ctrl Pts',(166.137589286737,-4.5476985602563,336.877824905842));
#44194=CARTESIAN_POINT('Ctrl Pts',(166.129878492616,-4.49216402145174,337.002409914796));
#44195=CARTESIAN_POINT('Ctrl Pts',(166.12215883249,-4.43656562806739,337.127138173764));
#44196=CARTESIAN_POINT('Ctrl Pts',(166.114439172364,-4.37581013511344,337.249455745313));
#44197=CARTESIAN_POINT('Ctrl Pts',(166.106719512238,-4.31015166500581,337.368918674659));
#44198=CARTESIAN_POINT('Ctrl Pts',(166.09899463244,-4.24444879971705,337.48846237924));
#44199=CARTESIAN_POINT('Ctrl Pts',(166.091269752641,-4.17383655953049,337.605147261037));
#44200=CARTESIAN_POINT('Ctrl Pts',(166.083544872843,-4.098612262968,337.718558548266));
#44201=CARTESIAN_POINT('Ctrl Pts',(166.075808780588,-4.02327878034587,337.832134448952));
#44202=CARTESIAN_POINT('Ctrl Pts',(166.068072688332,-3.94332011063052,337.942426952751));
#44203=CARTESIAN_POINT('Ctrl Pts',(166.060336596077,-3.85907388987416,338.049054242711));
#44204=CARTESIAN_POINT('Ctrl Pts',(166.05797793833,-3.83338805331583,338.081563845135));
#44205=CARTESIAN_POINT('Ctrl Pts',(166.055619280582,-3.80730391285455,338.113732997247));
#44206=CARTESIAN_POINT('Ctrl Pts',(166.053260622835,-3.78083169644808,338.145551580508));
#44207=CARTESIAN_POINT('Ctrl Pts',(166.045485544057,-3.69356868924297,338.250438350005));
#44208=CARTESIAN_POINT('Ctrl Pts',(166.037710465278,-3.60179987368437,338.351856870673));
#44209=CARTESIAN_POINT('Ctrl Pts',(166.0299353865,-3.50583135248403,338.449395539865));
#44210=CARTESIAN_POINT('Ctrl Pts',(166.022169875451,-3.40998092665856,338.546814181515));
#44211=CARTESIAN_POINT('Ctrl Pts',(166.014404364402,-3.30994134955729,338.640362195426));
#44212=CARTESIAN_POINT('Ctrl Pts',(166.006638853353,-3.206059476404,338.729660265528));
#44213=CARTESIAN_POINT('Ctrl Pts',(165.998881041831,-3.10228060243011,338.818869796335));
#44214=CARTESIAN_POINT('Ctrl Pts',(165.991123230308,-2.99466730832114,338.903837515938));
#44215=CARTESIAN_POINT('Ctrl Pts',(165.983365418786,-2.88360360762239,338.984220538149));
#44216=CARTESIAN_POINT('Ctrl Pts',(165.975613445263,-2.77262348588069,339.064543069586));
#44217=CARTESIAN_POINT('Ctrl Pts',(165.96786147174,-2.65819844120394,339.140287542697));
#44218=CARTESIAN_POINT('Ctrl Pts',(165.960109498217,-2.54074562661766,339.211151234915));
#44219=CARTESIAN_POINT('Ctrl Pts',(165.952360807659,-2.42334255336819,339.281984916317));
#44220=CARTESIAN_POINT('Ctrl Pts',(165.944612117102,-2.30291459452029,339.347941726467));
#44221=CARTESIAN_POINT('Ctrl Pts',(165.936863426544,-2.17990776780511,339.408762319105));
#44222=CARTESIAN_POINT('Ctrl Pts',(165.929116348166,-2.05692653368781,339.469570257511));
#44223=CARTESIAN_POINT('Ctrl Pts',(165.921369269788,-1.93136784911224,339.525243930854));
#44224=CARTESIAN_POINT('Ctrl Pts',(165.913622191411,-1.80370185461097,339.575570202955));
#44225=CARTESIAN_POINT('Ctrl Pts',(165.905875048105,-1.67603479014578,339.625896896839));
#44226=CARTESIAN_POINT('Ctrl Pts',(165.898127904799,-1.5462607441682,339.670875956744));
#44227=CARTESIAN_POINT('Ctrl Pts',(165.890380761493,-1.41486895833322,339.710342757512));
#44228=CARTESIAN_POINT('Ctrl Pts',(165.882631876465,-1.28344763283514,339.749818431254));
#44229=CARTESIAN_POINT('Ctrl Pts',(165.874882991437,-1.15040821803063,339.783779267421));
#44230=CARTESIAN_POINT('Ctrl Pts',(165.867134106409,-1.01625381442326,339.812110893067));
#44231=CARTESIAN_POINT('Ctrl Pts',(165.859376996634,-0.881957017945779,
339.840472590192));
#44232=CARTESIAN_POINT('Ctrl Pts',(165.851619886859,-0.746543251634799,
339.863193060476));
#44233=CARTESIAN_POINT('Ctrl Pts',(165.843862777085,-0.610525028347018,
339.880209242672));
#44234=CARTESIAN_POINT('Ctrl Pts',(165.836101522159,-0.474434121269662,
339.897234517772));
#44235=CARTESIAN_POINT('Ctrl Pts',(165.828340267232,-0.337738502948436,
339.908549398765));
#44236=CARTESIAN_POINT('Ctrl Pts',(165.820579012306,-0.200953465884062,
339.914142933111));
#44237=CARTESIAN_POINT('Ctrl Pts',(165.812805341902,-0.0639496173386181,
339.91974541529));
#44238=CARTESIAN_POINT('Ctrl Pts',(165.805031671497,0.0731435447082648,
339.919608262227));
#44239=CARTESIAN_POINT('Ctrl Pts',(165.797258001092,0.20981217803582,339.913772676106));
#44240=CARTESIAN_POINT('Ctrl Pts',(165.789846196915,0.340118853600547,339.908208737924));
#44241=CARTESIAN_POINT('Ctrl Pts',(165.782434392738,0.470039347797948,339.897464975405));
#44242=CARTESIAN_POINT('Ctrl Pts',(165.775022588561,0.599136456423764,339.881620485974));
#44243=CARTESIAN_POINT('Ctrl Pts',(165.767247509783,0.734560998904761,339.864999410918));
#44244=CARTESIAN_POINT('Ctrl Pts',(165.759472431004,0.869507368395578,339.842712437039));
#44245=CARTESIAN_POINT('Ctrl Pts',(165.751697352226,1.0034637897097,339.814794230831));
#44246=CARTESIAN_POINT('Ctrl Pts',(165.743931841177,1.13725536911931,339.786910379752));
#44247=CARTESIAN_POINT('Ctrl Pts',(165.736166330128,1.27005904521528,339.753409163228));
#44248=CARTESIAN_POINT('Ctrl Pts',(165.728400819079,1.4013681397591,339.714376989526));
#44249=CARTESIAN_POINT('Ctrl Pts',(165.720643007557,1.53254704095354,339.675383516337));
#44250=CARTESIAN_POINT('Ctrl Pts',(165.712885196034,1.66223393736663,339.630870110016));
#44251=CARTESIAN_POINT('Ctrl Pts',(165.705127384512,1.78993267692197,339.580974140353));
#44252=CARTESIAN_POINT('Ctrl Pts',(165.697375410989,1.91753531912598,339.53111571899));
#44253=CARTESIAN_POINT('Ctrl Pts',(165.689623437466,2.04315241988421,339.475882938388));
#44254=CARTESIAN_POINT('Ctrl Pts',(165.681871463943,2.16630366789437,339.415462770873));
#44255=CARTESIAN_POINT('Ctrl Pts',(165.674122773386,2.28940276127794,339.355068191335));
#44256=CARTESIAN_POINT('Ctrl Pts',(165.666374082828,2.41003772874752,339.289490766096));
#44257=CARTESIAN_POINT('Ctrl Pts',(165.65862539227,2.52774911471334,339.218965213837));
#44258=CARTESIAN_POINT('Ctrl Pts',(165.650878313893,2.645436009842,339.148454335008));
#44259=CARTESIAN_POINT('Ctrl Pts',(165.643131235515,2.76020019828136,339.072997577672));
#44260=CARTESIAN_POINT('Ctrl Pts',(165.635384157137,2.87160802925319,338.992874952816));
#44261=CARTESIAN_POINT('Ctrl Pts',(165.627637013831,2.98301679393007,338.912751656456));
#44262=CARTESIAN_POINT('Ctrl Pts',(165.619889870525,3.09106882770222,338.827962642798));
#44263=CARTESIAN_POINT('Ctrl Pts',(165.61214272722,3.19536093702955,338.738830237468));
#44264=CARTESIAN_POINT('Ctrl Pts',(165.604393842192,3.29967649343707,338.649677793282));
#44265=CARTESIAN_POINT('Ctrl Pts',(165.596644957164,3.40023014624294,338.556180268223));
#44266=CARTESIAN_POINT('Ctrl Pts',(165.588896072135,3.49665346024702,338.458698836476));
#44267=CARTESIAN_POINT('Ctrl Pts',(165.581138962361,3.59317911895288,338.361113936931));
#44268=CARTESIAN_POINT('Ctrl Pts',(165.573381852586,3.68556540612536,338.259536962084));
#44269=CARTESIAN_POINT('Ctrl Pts',(165.565624742811,3.77348194210339,338.154364768875));
#44270=CARTESIAN_POINT('Ctrl Pts',(165.557863487885,3.86144545786724,338.049136375008));
#44271=CARTESIAN_POINT('Ctrl Pts',(165.550102232959,3.94493422535332,337.940309244642));
#44272=CARTESIAN_POINT('Ctrl Pts',(165.542340978033,4.02366017999723,337.828310771186));
#44273=CARTESIAN_POINT('Ctrl Pts',(165.534567307628,4.10251207051185,337.716133136672));
#44274=CARTESIAN_POINT('Ctrl Pts',(165.526793637224,4.17658571196255,337.60077435056));
#44275=CARTESIAN_POINT('Ctrl Pts',(165.519019966819,4.2456376826352,337.482688810602));
#44276=CARTESIAN_POINT('Ctrl Pts',(165.511608162642,4.31147526745983,337.370100180939));
#44277=CARTESIAN_POINT('Ctrl Pts',(165.504196358465,4.37274804259686,337.25503319926));
#44278=CARTESIAN_POINT('Ctrl Pts',(165.496784554288,4.429285926475,337.137898324063));
#44279=CARTESIAN_POINT('Ctrl Pts',(165.489009475509,4.48859490045991,337.015022319705));
#44280=CARTESIAN_POINT('Ctrl Pts',(165.481234396731,4.54288053240625,336.889482278253));
#44281=CARTESIAN_POINT('Ctrl Pts',(165.473459317953,4.59189502318759,336.76172732241));
#44282=CARTESIAN_POINT('Ctrl Pts',(165.465693806904,4.64084919851758,336.634129577173));
#44283=CARTESIAN_POINT('Ctrl Pts',(165.457928295855,4.68454500023399,336.504322702141));
#44284=CARTESIAN_POINT('Ctrl Pts',(165.450162784806,4.72278089822452,336.372779534326));
#44285=CARTESIAN_POINT('Ctrl Pts',(165.442404973283,4.76097888521093,336.241366791946));
#44286=CARTESIAN_POINT('Ctrl Pts',(165.434647161761,4.79372763326548,336.108221555664));
#44287=CARTESIAN_POINT('Ctrl Pts',(165.426889350239,4.82087416321797,335.973835389025));
#44288=CARTESIAN_POINT('Ctrl Pts',(165.419137376716,4.84800026454584,335.839550352237));
#44289=CARTESIAN_POINT('Ctrl Pts',(165.411385403193,4.86953246212534,335.704026625446));
#44290=CARTESIAN_POINT('Ctrl Pts',(165.40363342967,4.88536806097013,335.567769294127));
#44291=CARTESIAN_POINT('Ctrl Pts',(165.395884739112,4.90119695342938,335.431569667868));
#44292=CARTESIAN_POINT('Ctrl Pts',(165.388136048555,4.91133400044307,335.29463744246));
#44293=CARTESIAN_POINT('Ctrl Pts',(165.380387357997,4.91572794417595,335.157486003656));
#44294=CARTESIAN_POINT('Ctrl Pts',(165.372640279619,4.92012097371215,335.020363100355));
#44295=CARTESIAN_POINT('Ctrl Pts',(165.364893201241,4.91877326420113,334.883021464807));
#44296=CARTESIAN_POINT('Ctrl Pts',(165.357146122864,4.91168560953754,334.745977293216));
#44297=CARTESIAN_POINT('Ctrl Pts',(165.349398979558,4.90459789547258,334.608931973063));
#44298=CARTESIAN_POINT('Ctrl Pts',(165.341651836252,4.89177016049177,334.472184512192));
#44299=CARTESIAN_POINT('Ctrl Pts',(165.333904692946,4.87325526393051,334.336248393543));
#44300=CARTESIAN_POINT('Ctrl Pts',(165.326155807918,4.85473620482745,334.20028171357));
#44301=CARTESIAN_POINT('Ctrl Pts',(165.31840692289,4.83052749262428,334.065127126011));
#44302=CARTESIAN_POINT('Ctrl Pts',(165.310658037862,4.80073346496936,333.931289907962));
#44303=CARTESIAN_POINT('Ctrl Pts',(165.302900928087,4.77090781362567,333.797310633707));
#44304=CARTESIAN_POINT('Ctrl Pts',(165.295143818312,4.73548508954091,333.664651904274));
#44305=CARTESIAN_POINT('Ctrl Pts',(165.287386708538,4.69462023078815,333.533806305028));
#44306=CARTESIAN_POINT('Ctrl Pts',(165.279625453611,4.65373353516151,333.402890786078));
#44307=CARTESIAN_POINT('Ctrl Pts',(165.271864198685,4.60739904218282,333.273790695604));
#44308=CARTESIAN_POINT('Ctrl Pts',(165.264102943759,4.5558202678229,333.146979560341));
#44309=CARTESIAN_POINT('Ctrl Pts',(165.256329273354,4.50415898423348,333.019965568589));
#44310=CARTESIAN_POINT('Ctrl Pts',(165.24855560295,4.44723681765391,332.895248204751));
#44311=CARTESIAN_POINT('Ctrl Pts',(165.240781932545,4.38530415139085,332.773278068035));
#44312=CARTESIAN_POINT('Ctrl Pts',(165.233370128368,4.32625446564266,332.656985670528));
#44313=CARTESIAN_POINT('Ctrl Pts',(165.225958324191,4.26265040036041,332.543190740389));
#44314=CARTESIAN_POINT('Ctrl Pts',(165.218546520014,4.19474507795339,332.432258425486));
#44315=CARTESIAN_POINT('Ctrl Pts',(165.210771441235,4.12351151341542,332.315888987379));
#44316=CARTESIAN_POINT('Ctrl Pts',(165.202996362457,4.04731928463488,332.202302121427));
#44317=CARTESIAN_POINT('Ctrl Pts',(165.195221283678,3.96641197014625,332.091949253266));
#44318=CARTESIAN_POINT('Ctrl Pts',(165.187455772629,3.88560421725891,331.981732181335));
#44319=CARTESIAN_POINT('Ctrl Pts',(165.17969026158,3.80009315230977,331.874741501066));
#44320=CARTESIAN_POINT('Ctrl Pts',(165.171924750531,3.7101673345222,331.771402562668));
#44321=CARTESIAN_POINT('Ctrl Pts',(165.164166939009,3.62033067844447,331.668166085129));
#44322=CARTESIAN_POINT('Ctrl Pts',(165.156409127487,3.52608823542148,331.568574437002));
#44323=CARTESIAN_POINT('Ctrl Pts',(165.148651315965,3.42777058591576,331.473022274974));
#44324=CARTESIAN_POINT('Ctrl Pts',(165.140899342442,3.32952692355933,331.377542018978));
#44325=CARTESIAN_POINT('Ctrl Pts',(165.133147368919,3.22721443805593,331.286095469747));
#44326=CARTESIAN_POINT('Ctrl Pts',(165.125395395396,3.12120229240839,331.19904231642));
#44327=CARTESIAN_POINT('Ctrl Pts',(165.117646704838,3.01523504296749,331.112026030155));
#44328=CARTESIAN_POINT('Ctrl Pts',(165.10989801428,2.90557155110333,331.029399686719));
#44329=CARTESIAN_POINT('Ctrl Pts',(165.102149323723,2.79261579529406,330.951484212409));
#44330=CARTESIAN_POINT('Ctrl Pts',(165.094402245345,2.6796835408733,330.873584949064));
#44331=CARTESIAN_POINT('Ctrl Pts',(165.086655166967,2.56346070653789,330.800394827088));
#44332=CARTESIAN_POINT('Ctrl Pts',(165.078908088589,2.44438180230996,330.732192522262));
#44333=CARTESIAN_POINT('Ctrl Pts',(165.071160945283,2.32530190008611,330.663989645835));
#44334=CARTESIAN_POINT('Ctrl Pts',(165.063413801977,2.20336621940721,330.600774864204));
#44335=CARTESIAN_POINT('Ctrl Pts',(165.055666658672,2.07903516425226,330.542781601907));
#44336=CARTESIAN_POINT('Ctrl Pts',(165.047917773643,1.95467615683688,330.484775301493));
#44337=CARTESIAN_POINT('Ctrl Pts',(165.040168888615,1.82792105749378,330.431993021559));
#44338=CARTESIAN_POINT('Ctrl Pts',(165.032420003587,1.69925122759994,330.384620456777));
#44339=CARTESIAN_POINT('Ctrl Pts',(165.024662893813,1.57044482621895,330.337197610266));
#44340=CARTESIAN_POINT('Ctrl Pts',(165.016905784038,1.43972000193101,330.295196084207));
#44341=CARTESIAN_POINT('Ctrl Pts',(165.009148674263,1.30757482616058,330.258752154075));
#44342=CARTESIAN_POINT('Ctrl Pts',(165.001387419337,1.17535903623344,330.222288749472));
#44343=CARTESIAN_POINT('Ctrl Pts',(164.993626164411,1.04172176310057,330.191388946403));
#44344=CARTESIAN_POINT('Ctrl Pts',(164.985864909485,0.907171339665501,330.166137856435));
#44345=CARTESIAN_POINT('Ctrl Pts',(164.97809123908,0.772405679402744,330.140846372952));
#44346=CARTESIAN_POINT('Ctrl Pts',(164.970317568675,0.636724336893146,330.121221715357));
#44347=CARTESIAN_POINT('Ctrl Pts',(164.962543898271,0.500641727399296,330.107297176071));
#44348=CARTESIAN_POINT('Ctrl Pts',(164.955132094093,0.370893796117201,330.094020827439));
#44349=CARTESIAN_POINT('Ctrl Pts',(164.947720289916,0.240781402330473,330.085925876618));
#44350=CARTESIAN_POINT('Ctrl Pts',(164.940308485739,0.11074858573003,330.082997070038));
#44351=CARTESIAN_POINT('Ctrl Pts',(164.932533406961,-0.0256575265601337,
330.079924713922));
#44352=CARTESIAN_POINT('Ctrl Pts',(164.924758328182,-0.162407132311235,
330.082528013814));
#44353=CARTESIAN_POINT('Ctrl Pts',(164.916983249404,-0.298988803753761,
330.090846431641));
#44354=CARTESIAN_POINT('Ctrl Pts',(164.909217738355,-0.43540240275471,330.099154613126));
#44355=CARTESIAN_POINT('Ctrl Pts',(164.901452227306,-0.571648092207341,
330.113163895723));
#44356=CARTESIAN_POINT('Ctrl Pts',(164.893686716257,-0.707212030092754,
330.13286180523));
#44357=CARTESIAN_POINT('Ctrl Pts',(164.885928904735,-0.842641555938794,
330.152540184202));
#44358=CARTESIAN_POINT('Ctrl Pts',(164.878171093213,-0.977390291093121,
330.177895909745));
#44359=CARTESIAN_POINT('Ctrl Pts',(164.87041328169,-1.11094746427157,330.208864561074));
#44360=CARTESIAN_POINT('Ctrl Pts',(164.862661308167,-1.24440413144189,330.239809907511));
#44361=CARTESIAN_POINT('Ctrl Pts',(164.854909334644,-1.37667064221152,330.276359684322));
#44362=CARTESIAN_POINT('Ctrl Pts',(164.847157361121,-1.50724475102736,330.318398102893));
#44363=CARTESIAN_POINT('Ctrl Pts',(164.839408670564,-1.63776356163028,330.360418718168));
#44364=CARTESIAN_POINT('Ctrl Pts',(164.831659980006,-1.76659102451878,330.407923232513));
#44365=CARTESIAN_POINT('Ctrl Pts',(164.823911289449,-1.893238649988,330.46074560344));
#44366=CARTESIAN_POINT('Ctrl Pts',(164.816164211071,-2.01985992536101,330.513556984231));
#44367=CARTESIAN_POINT('Ctrl Pts',(164.808417132693,-2.14430190489733,330.57168387048));
#44368=CARTESIAN_POINT('Ctrl Pts',(164.800670054315,-2.2660951058813,330.634911680893));
#44369=CARTESIAN_POINT('Ctrl Pts',(164.792922911009,-2.38788932760944,330.698140021217));
#44370=CARTESIAN_POINT('Ctrl Pts',(164.785175767704,-2.50703437959486,330.766469190879));
#44371=CARTESIAN_POINT('Ctrl Pts',(164.777428624398,-2.62308481915098,330.839638345764));
#44372=CARTESIAN_POINT('Ctrl Pts',(164.76967973937,-2.73916134930914,330.912823950628));
#44373=CARTESIAN_POINT('Ctrl Pts',(164.761930854342,-2.85214155202689,330.990851497547));
#44374=CARTESIAN_POINT('Ctrl Pts',(164.754181969314,-2.96160878042939,331.073416689514));
#44375=CARTESIAN_POINT('Ctrl Pts',(164.746424859539,-3.07119219847979,331.15606951703));
#44376=CARTESIAN_POINT('Ctrl Pts',(164.738667749764,-3.17725488121721,331.243269374868));
#44377=CARTESIAN_POINT('Ctrl Pts',(164.730910639989,-3.27941269666047,331.33467117062));
#44378=CARTESIAN_POINT('Ctrl Pts',(164.723149385063,-3.38162510197416,331.42612180857));
#44379=CARTESIAN_POINT('Ctrl Pts',(164.715388130137,-3.47992820219039,331.521778586103));
#44380=CARTESIAN_POINT('Ctrl Pts',(164.707626875211,-3.57397533707553,331.621260093988));
#44381=CARTESIAN_POINT('Ctrl Pts',(164.699853204806,-3.66817291672646,331.720900739865));
#44382=CARTESIAN_POINT('Ctrl Pts',(164.692079534402,-3.75810066979844,331.824378047128));
#44383=CARTESIAN_POINT('Ctrl Pts',(164.684305863997,-3.84345222036665,331.931277449449));
#44384=CARTESIAN_POINT('Ctrl Pts',(164.67689405982,-3.92483063572159,332.033200658874));
#44385=CARTESIAN_POINT('Ctrl Pts',(164.669482255643,-4.00204913469065,332.138234304259));
#44386=CARTESIAN_POINT('Ctrl Pts',(164.662070451466,-4.07488024897162,332.245996728571));
#44387=CARTESIAN_POINT('Ctrl Pts',(164.654169951851,-4.15251346438675,332.360864441127));
#44388=CARTESIAN_POINT('Ctrl Pts',(164.646269452237,-4.22540144646196,332.479187903196));
#44389=CARTESIAN_POINT('Ctrl Pts',(164.638368952622,-4.29322723335163,332.600545273336));
#44390=CARTESIAN_POINT('Ctrl Pts',(164.630478996904,-4.360962500893,332.721740681625));
#44391=CARTESIAN_POINT('Ctrl Pts',(164.622589041186,-4.42364883999927,332.845961615013));
#44392=CARTESIAN_POINT('Ctrl Pts',(164.614699085468,-4.4810116748555,332.972756198108));
#44393=CARTESIAN_POINT('Ctrl Pts',(164.606818151548,-4.53830891797762,333.099405797494));
#44394=CARTESIAN_POINT('Ctrl Pts',(164.598937217627,-4.59029462212641,333.228622849245));
#44395=CARTESIAN_POINT('Ctrl Pts',(164.591056283707,-4.63673949099087,333.35992989321));
#44396=CARTESIAN_POINT('Ctrl Pts',(164.583179614105,-4.68315922885682,333.491165887838));
#44397=CARTESIAN_POINT('Ctrl Pts',(164.575302944504,-4.72404395697051,333.624489278899));
#44398=CARTESIAN_POINT('Ctrl Pts',(164.567426274903,-4.75921185762725,333.759401129809));
#44399=CARTESIAN_POINT('Ctrl Pts',(164.559559820631,-4.79433414868988,333.89413801222));
#44400=CARTESIAN_POINT('Ctrl Pts',(164.551693366359,-4.82375430849274,334.030458883297));
#44401=CARTESIAN_POINT('Ctrl Pts',(164.543826912088,-4.8473404005135,334.167849710659));
#44402=CARTESIAN_POINT('Ctrl Pts',(164.535945134821,-4.87097243566829,334.305508160364));
#44403=CARTESIAN_POINT('Ctrl Pts',(164.528063357555,-4.88874754373616,334.444240376606));
#44404=CARTESIAN_POINT('Ctrl Pts',(164.520181580289,-4.90058419455674,334.583517569926));
#44405=CARTESIAN_POINT('Ctrl Pts',(164.512299803023,-4.91242084537732,334.722794763246));
#44406=CARTESIAN_POINT('Ctrl Pts',(164.504418025756,-4.91831898961313,334.862616557649));
#44407=CARTESIAN_POINT('Ctrl Pts',(164.49653624849,-4.91824939077894,335.002447979287));
#44408=CARTESIAN_POINT('',(167.996536248449,-4.91824997640728,334.999518263764));
#44409=CARTESIAN_POINT('Ctrl Pts',(167.996536248449,-4.91824997640728,334.999518263764));
#44410=CARTESIAN_POINT('Ctrl Pts',(167.988782474437,-4.91826330456105,335.135591050191));
#44411=CARTESIAN_POINT('Ctrl Pts',(167.981028700426,-4.91262528295511,335.271884721958));
#44412=CARTESIAN_POINT('Ctrl Pts',(167.973274926414,-4.90130688742149,335.407889516677));
#44413=CARTESIAN_POINT('Ctrl Pts',(167.965530681001,-4.89000240104323,335.543727175354));
#44414=CARTESIAN_POINT('Ctrl Pts',(167.957786435588,-4.87303146095585,335.679276275156));
#44415=CARTESIAN_POINT('Ctrl Pts',(167.950042190175,-4.8504170187412,335.814025679451));
#44416=CARTESIAN_POINT('Ctrl Pts',(167.942305583009,-4.82782488143851,335.948642178695));
#44417=CARTESIAN_POINT('Ctrl Pts',(167.934568975844,-4.79960038272873,336.082460166602));
#44418=CARTESIAN_POINT('Ctrl Pts',(167.926832368679,-4.76581834802965,336.214972648286));
#44419=CARTESIAN_POINT('Ctrl Pts',(167.919101516249,-4.7320614414861,336.347386562958));
#44420=CARTESIAN_POINT('Ctrl Pts',(167.911370663819,-4.69275532322838,336.478496524548));
#44421=CARTESIAN_POINT('Ctrl Pts',(167.903639811389,-4.64802599510974,336.607805153395));
#44422=CARTESIAN_POINT('Ctrl Pts',(167.895912112537,-4.60331491303071,336.737061034516));
#44423=CARTESIAN_POINT('Ctrl Pts',(167.888184413685,-4.55318514861906,336.864516673185));
#44424=CARTESIAN_POINT('Ctrl Pts',(167.880456714834,-4.49781264724263,336.989689536788));
#44425=CARTESIAN_POINT('Ctrl Pts',(167.872730512087,-4.44245086614406,337.114838166559));
#44426=CARTESIAN_POINT('Ctrl Pts',(167.86500430934,-4.38184852582045,337.237704540794));
#44427=CARTESIAN_POINT('Ctrl Pts',(167.857278106594,-4.31622967029951,337.357826222546));
#44428=CARTESIAN_POINT('Ctrl Pts',(167.849551703081,-4.25060910966695,337.47795102567));
#44429=CARTESIAN_POINT('Ctrl Pts',(167.841825299568,-4.17997196292442,337.595330649212));
#44430=CARTESIAN_POINT('Ctrl Pts',(167.834098896056,-4.10458796687714,337.709527760453));
#44431=CARTESIAN_POINT('Ctrl Pts',(167.826370595115,-4.02918545824734,337.823752915889));
#44432=CARTESIAN_POINT('Ctrl Pts',(167.818642294175,-3.9490339976311,337.934793675944));
#44433=CARTESIAN_POINT('Ctrl Pts',(167.810913993234,-3.86444607508734,338.042242527354));
#44434=CARTESIAN_POINT('Ctrl Pts',(167.803177450501,-3.77976794434275,338.149805966843));
#44435=CARTESIAN_POINT('Ctrl Pts',(167.795440907768,-3.69064414589996,338.253769537759));
#44436=CARTESIAN_POINT('Ctrl Pts',(167.787704365035,-3.5974271314745,338.3537592484));
#44437=CARTESIAN_POINT('Ctrl Pts',(167.779963499509,-3.50415803204282,338.453804828292));
#44438=CARTESIAN_POINT('Ctrl Pts',(167.772222633983,-3.40679144008804,338.549871848678));
#44439=CARTESIAN_POINT('Ctrl Pts',(167.764481768456,-3.30571516406244,338.641624680907));
#44440=CARTESIAN_POINT('Ctrl Pts',(167.756728880654,-3.20448190729009,338.733520013716));
#44441=CARTESIAN_POINT('Ctrl Pts',(167.748975992852,-3.0995277583632,338.821087521177));
#44442=CARTESIAN_POINT('Ctrl Pts',(167.74122310505,-2.99127252594288,338.904032753198));
#44443=CARTESIAN_POINT('Ctrl Pts',(167.73504501286,-2.90500650183863,338.97012983899));
#44444=CARTESIAN_POINT('Ctrl Pts',(167.728866920669,-2.81664490383749,339.033292524293));
#44445=CARTESIAN_POINT('Ctrl Pts',(167.722688828479,-2.72641170751432,339.093392512773));
#44446=CARTESIAN_POINT('Ctrl Pts',(167.7149137497,-2.6128539637631,339.169027859512));
#44447=CARTESIAN_POINT('Ctrl Pts',(167.707138670922,-2.49596701032929,339.240053713681));
#44448=CARTESIAN_POINT('Ctrl Pts',(167.699363592144,-2.37616164720912,339.306162896226));
#44449=CARTESIAN_POINT('Ctrl Pts',(167.691598081095,-2.25650371221542,339.372190727213));
#44450=CARTESIAN_POINT('Ctrl Pts',(167.683832570046,-2.1339348521281,339.433313737856));
#44451=CARTESIAN_POINT('Ctrl Pts',(167.676067058997,-2.00889571584567,339.489267319436));
#44452=CARTESIAN_POINT('Ctrl Pts',(167.668309247474,-1.88398055623153,339.545165422876));
#44453=CARTESIAN_POINT('Ctrl Pts',(167.660551435952,-1.75660034912292,339.595904138669));
#44454=CARTESIAN_POINT('Ctrl Pts',(167.65279362443,-1.62722096553022,339.641264374267));
#44455=CARTESIAN_POINT('Ctrl Pts',(167.645041650907,-1.49793894402527,339.68659047485));
#44456=CARTESIAN_POINT('Ctrl Pts',(167.637289677384,-1.36666110793366,339.726546022741));
#44457=CARTESIAN_POINT('Ctrl Pts',(167.629537703861,-1.23387363341416,339.76095987373));
#44458=CARTESIAN_POINT('Ctrl Pts',(167.621789013303,-1.10114239446967,339.795359150432));
#44459=CARTESIAN_POINT('Ctrl Pts',(167.614040322746,-0.966903166271453,
339.824221300216));
#44460=CARTESIAN_POINT('Ctrl Pts',(167.606291632188,-0.83165741650632,339.847424986946));
#44461=CARTESIAN_POINT('Ctrl Pts',(167.59854455381,-0.696439805749181,339.870623845955));
#44462=CARTESIAN_POINT('Ctrl Pts',(167.590797475432,-0.560216474970463,
339.88816651757));
#44463=CARTESIAN_POINT('Ctrl Pts',(167.583050397055,-0.423498830134245,
339.899982837049));
#44464=CARTESIAN_POINT('Ctrl Pts',(167.575303253749,-0.286780039472225,
339.911799255561));
#44465=CARTESIAN_POINT('Ctrl Pts',(167.567556110443,-0.149567315912039,
339.917889192556));
#44466=CARTESIAN_POINT('Ctrl Pts',(167.559808967137,-0.0123765342951703,
339.918234427505));
#44467=CARTESIAN_POINT('Ctrl Pts',(167.552060082109,0.124845090721558,339.918579740071));
#44468=CARTESIAN_POINT('Ctrl Pts',(167.544311197081,0.26204437318215,339.913177779605));
#44469=CARTESIAN_POINT('Ctrl Pts',(167.536562312053,0.398706490519899,339.902062443188));
#44470=CARTESIAN_POINT('Ctrl Pts',(167.528805202278,0.535513662441278,339.890935308839));
#44471=CARTESIAN_POINT('Ctrl Pts',(167.521048092503,0.671782140103341,339.874082716395));
#44472=CARTESIAN_POINT('Ctrl Pts',(167.513290982729,0.807002717186098,339.851590427577));
#44473=CARTESIAN_POINT('Ctrl Pts',(167.505529727803,0.942295551821779,339.829086119598));
#44474=CARTESIAN_POINT('Ctrl Pts',(167.497768472876,1.0765389877383,339.800936190408));
#44475=CARTESIAN_POINT('Ctrl Pts',(167.49000721795,1.20923601932964,339.767277138163));
#44476=CARTESIAN_POINT('Ctrl Pts',(167.482233547546,1.34214532292559,339.733564242405));
#44477=CARTESIAN_POINT('Ctrl Pts',(167.474459877141,1.47350290420733,339.694324724941));
#44478=CARTESIAN_POINT('Ctrl Pts',(167.466686206736,1.60282802557411,339.649744657821));
#44479=CARTESIAN_POINT('Ctrl Pts',(167.459274402559,1.72613303142783,339.60723980355));
#44480=CARTESIAN_POINT('Ctrl Pts',(167.451862598382,1.84759027292765,339.559880520056));
#44481=CARTESIAN_POINT('Ctrl Pts',(167.444450794205,1.96680327628418,339.507867337766));
#44482=CARTESIAN_POINT('Ctrl Pts',(167.436675715427,2.09185926405209,339.453304834473));
#44483=CARTESIAN_POINT('Ctrl Pts',(167.428900636648,2.21484065756744,339.39344826681));
#44484=CARTESIAN_POINT('Ctrl Pts',(167.42112555787,2.3352668359619,339.328476853046));
#44485=CARTESIAN_POINT('Ctrl Pts',(167.413360046821,2.45554482227723,339.263585390743));
#44486=CARTESIAN_POINT('Ctrl Pts',(167.405594535772,2.57327350912233,339.1935917897));
#44487=CARTESIAN_POINT('Ctrl Pts',(167.397829024723,2.68799192097653,339.118723406016));
#44488=CARTESIAN_POINT('Ctrl Pts',(167.3900712132,2.80259658919157,339.043929254552));
#44489=CARTESIAN_POINT('Ctrl Pts',(167.382313401678,2.91419659690643,338.964270151358));
#44490=CARTESIAN_POINT('Ctrl Pts',(167.374555590156,3.02235559498915,338.880019293758));
#44491=CARTESIAN_POINT('Ctrl Pts',(167.366803616633,3.13043319999614,338.7958318376));
#44492=CARTESIAN_POINT('Ctrl Pts',(167.35905164311,3.23507464246211,338.707059744154));
#44493=CARTESIAN_POINT('Ctrl Pts',(167.351299669587,3.33587290575179,338.61401923337));
#44494=CARTESIAN_POINT('Ctrl Pts',(167.343550979029,3.43662848091667,338.521018125299));
#44495=CARTESIAN_POINT('Ctrl Pts',(167.335802288472,3.53354382744071,338.423752459797));
#44496=CARTESIAN_POINT('Ctrl Pts',(167.328053597914,3.62624553823805,338.322578269794));
#44497=CARTESIAN_POINT('Ctrl Pts',(167.320306519536,3.71892796167028,338.221425129927));
#44498=CARTESIAN_POINT('Ctrl Pts',(167.312559441158,3.80739822926484,338.116365371086));
#44499=CARTESIAN_POINT('Ctrl Pts',(167.30481236278,3.89132058688308,338.007791075291));
#44500=CARTESIAN_POINT('Ctrl Pts',(167.297065219475,3.97524364785143,337.899215869538));
#44501=CARTESIAN_POINT('Ctrl Pts',(167.289318076169,4.05461848377652,337.78712637734));
#44502=CARTESIAN_POINT('Ctrl Pts',(167.281570932863,4.12915060314886,337.671946548682));
#44503=CARTESIAN_POINT('Ctrl Pts',(167.273822047835,4.20369947892386,337.556740825154));
#44504=CARTESIAN_POINT('Ctrl Pts',(167.266073162807,4.27340325935474,337.438443710742));
#44505=CARTESIAN_POINT('Ctrl Pts',(167.258324277779,4.33801184918885,337.317506474381));
#44506=CARTESIAN_POINT('Ctrl Pts',(167.250567168004,4.40268901524788,337.196440873988));
#44507=CARTESIAN_POINT('Ctrl Pts',(167.242810058229,4.46226000307407,337.072729899188));
#44508=CARTESIAN_POINT('Ctrl Pts',(167.235052948455,4.51652137076929,336.946848163028));
#44509=CARTESIAN_POINT('Ctrl Pts',(167.227291693528,4.57081173400451,336.820899159692));
#44510=CARTESIAN_POINT('Ctrl Pts',(167.219530438602,4.61978668405707,336.692777448544));
#44511=CARTESIAN_POINT('Ctrl Pts',(167.211769183676,4.66329204688818,336.562974839186));
#44512=CARTESIAN_POINT('Ctrl Pts',(167.203995513271,4.70686700412138,336.432964587956));
#44513=CARTESIAN_POINT('Ctrl Pts',(167.196221842867,4.74495478127576,336.301268441003));
#44514=CARTESIAN_POINT('Ctrl Pts',(167.188448172462,4.77745169560569,336.168391355092));
#44515=CARTESIAN_POINT('Ctrl Pts',(167.181036368285,4.80843587075487,336.041699729501));
#44516=CARTESIAN_POINT('Ctrl Pts',(167.173624564108,4.83433792148842,335.913934918175));
#44517=CARTESIAN_POINT('Ctrl Pts',(167.166212759931,4.85511192340498,335.785538842904));
#44518=CARTESIAN_POINT('Ctrl Pts',(167.158437681153,4.87690412103831,335.65084969351));
#44519=CARTESIAN_POINT('Ctrl Pts',(167.150662602374,4.89312174500852,335.515040192678));
#44520=CARTESIAN_POINT('Ctrl Pts',(167.142887523596,4.90365541225215,335.37861149004));
#44521=CARTESIAN_POINT('Ctrl Pts',(167.135122012547,4.91417611714764,335.242350671605));
#44522=CARTESIAN_POINT('Ctrl Pts',(167.127356501498,4.91902675250529,335.10547255345));
#44523=CARTESIAN_POINT('Ctrl Pts',(167.119590990449,4.91814904661359,334.968487815153));
#44524=CARTESIAN_POINT('Ctrl Pts',(167.111833178926,4.91727221096984,334.831638897623));
#44525=CARTESIAN_POINT('Ctrl Pts',(167.104075367404,4.91067833942356,334.694683958678));
#44526=CARTESIAN_POINT('Ctrl Pts',(167.096317555882,4.8983610358791,334.558137776359));
#44527=CARTESIAN_POINT('Ctrl Pts',(167.088565582359,4.88605300149619,334.421694349372));
#44528=CARTESIAN_POINT('Ctrl Pts',(167.080813608836,4.86803014309089,334.285659454471));
#44529=CARTESIAN_POINT('Ctrl Pts',(167.073061635313,4.84433811671005,334.150546485386));
#44530=CARTESIAN_POINT('Ctrl Pts',(167.065312944755,4.82065612391641,334.015490736724));
#44531=CARTESIAN_POINT('Ctrl Pts',(167.057564254198,4.7913098057294,333.881356521528));
#44532=CARTESIAN_POINT('Ctrl Pts',(167.04981556364,4.75639648583532,333.74865051563));
#44533=CARTESIAN_POINT('Ctrl Pts',(167.042068485262,4.72149042994909,333.615972120325));
#44534=CARTESIAN_POINT('Ctrl Pts',(167.034321406885,4.68101977560688,333.484721721038));
#44535=CARTESIAN_POINT('Ctrl Pts',(167.026574328507,4.63513253711278,333.355393838666));
#44536=CARTESIAN_POINT('Ctrl Pts',(167.018827185201,4.58924491403937,333.226064872401));
#44537=CARTESIAN_POINT('Ctrl Pts',(167.011080041895,4.53794074697179,333.098658823561));
#44538=CARTESIAN_POINT('Ctrl Pts',(167.003332898589,4.48141717824412,332.973652760004));
#44539=CARTESIAN_POINT('Ctrl Pts',(166.995584013561,4.42488090181821,332.84861859243));
#44540=CARTESIAN_POINT('Ctrl Pts',(166.987835128533,4.36312304974399,332.725985839905));
#44541=CARTESIAN_POINT('Ctrl Pts',(166.980086243505,4.29638776280485,332.606209020378));
#44542=CARTESIAN_POINT('Ctrl Pts',(166.97232913373,4.22958164234264,332.486305068497));
#44543=CARTESIAN_POINT('Ctrl Pts',(166.964572023956,4.15778772407131,332.369263446944));
#44544=CARTESIAN_POINT('Ctrl Pts',(166.956814914181,4.08129502614167,332.255512074705));
#44545=CARTESIAN_POINT('Ctrl Pts',(166.949053659255,4.00476145295993,332.141699917369));
#44546=CARTESIAN_POINT('Ctrl Pts',(166.941292404328,3.92352432835442,332.031181827511));
#44547=CARTESIAN_POINT('Ctrl Pts',(166.933531149402,3.83791379309335,331.924353599764));
#44548=CARTESIAN_POINT('Ctrl Pts',(166.925757478998,3.7521663088763,331.817354481668));
#44549=CARTESIAN_POINT('Ctrl Pts',(166.917983808593,3.66203169098352,331.714057315452));
#44550=CARTESIAN_POINT('Ctrl Pts',(166.910210138188,3.56787845964979,331.614822551229));
#44551=CARTESIAN_POINT('Ctrl Pts',(166.902798334011,3.47810808388649,331.520207189155));
#44552=CARTESIAN_POINT('Ctrl Pts',(166.895386529834,3.38468501420987,331.429284731544));
#44553=CARTESIAN_POINT('Ctrl Pts',(166.887974725657,3.28795601975188,331.342332946443));
#44554=CARTESIAN_POINT('Ctrl Pts',(166.880199646879,3.18648604913493,331.251119395338));
#44555=CARTESIAN_POINT('Ctrl Pts',(166.8724245681,3.08105722941441,331.163987335706));
#44556=CARTESIAN_POINT('Ctrl Pts',(166.864649489322,2.9720317945545,331.08129995092));
#44557=CARTESIAN_POINT('Ctrl Pts',(166.856883978273,2.86314052243333,330.998714318226));
#44558=CARTESIAN_POINT('Ctrl Pts',(166.849118467224,2.75066174983152,330.920562711671));
#44559=CARTESIAN_POINT('Ctrl Pts',(166.841352956175,2.63499338393629,330.847170491206));
#44560=CARTESIAN_POINT('Ctrl Pts',(166.833595144653,2.51943970356208,330.77385103934));
#44561=CARTESIAN_POINT('Ctrl Pts',(166.82583733313,2.40070305134741,330.705281790662));
#44562=CARTESIAN_POINT('Ctrl Pts',(166.818079521608,2.2792128538355,330.641746699719));
#44563=CARTESIAN_POINT('Ctrl Pts',(166.810327548085,2.15781408154979,330.578259420947));
#44564=CARTESIAN_POINT('Ctrl Pts',(166.802575574562,2.03366623341493,330.519798939769));
#44565=CARTESIAN_POINT('Ctrl Pts',(166.794823601039,1.90722574027958,330.466604689847));
#44566=CARTESIAN_POINT('Ctrl Pts',(166.787074910481,1.7808387947685,330.413432967722));
#44567=CARTESIAN_POINT('Ctrl Pts',(166.779326219924,1.6521614949197,330.3655231923));
#44568=CARTESIAN_POINT('Ctrl Pts',(166.771577529366,1.52167258268121,330.323067713381));
#44569=CARTESIAN_POINT('Ctrl Pts',(166.763830450988,1.39121081975087,330.28062106768));
#44570=CARTESIAN_POINT('Ctrl Pts',(166.756083372611,1.25893856561594,330.243626582119));
#44571=CARTESIAN_POINT('Ctrl Pts',(166.748336294233,1.12535177248105,330.212227401946));
#44572=CARTESIAN_POINT('Ctrl Pts',(166.740589150927,0.991763859760445,330.180827958618));
#44573=CARTESIAN_POINT('Ctrl Pts',(166.732842007621,0.856861766570149,330.155024003647));
#44574=CARTESIAN_POINT('Ctrl Pts',(166.725094864315,0.721153354477636,330.13490792463));
#44575=CARTESIAN_POINT('Ctrl Pts',(166.717345979287,0.585414432252612,330.114787323092));
#44576=CARTESIAN_POINT('Ctrl Pts',(166.709597094259,0.448869216977219,330.10035719939));
#44577=CARTESIAN_POINT('Ctrl Pts',(166.701848209231,0.312032041077469,330.091658216073));
#44578=CARTESIAN_POINT('Ctrl Pts',(166.694091099456,0.175049624785287,330.082949999566));
#44579=CARTESIAN_POINT('Ctrl Pts',(166.686333989682,0.037775019537325,330.079985099827));
#44580=CARTESIAN_POINT('Ctrl Pts',(166.678576879907,-0.0992755241577299,
330.082752046845));
#44581=CARTESIAN_POINT('Ctrl Pts',(166.670815624981,-0.236399303281239,
330.085520472432));
#44582=CARTESIAN_POINT('Ctrl Pts',(166.663054370055,-0.373298392352362,
330.094026823681));
#44583=CARTESIAN_POINT('Ctrl Pts',(166.655293115128,-0.509461301106,330.108207665367));
#44584=CARTESIAN_POINT('Ctrl Pts',(166.647519444724,-0.645842026138325,
330.122411191778));
#44585=CARTESIAN_POINT('Ctrl Pts',(166.639745774319,-0.781483830623061,
330.142307291072));
#44586=CARTESIAN_POINT('Ctrl Pts',(166.631972103914,-0.915884176925122,
330.167781126961));
#44587=CARTESIAN_POINT('Ctrl Pts',(166.624560299737,-1.04402815477236,330.19206914966));
#44588=CARTESIAN_POINT('Ctrl Pts',(166.61714849556,-1.17104337273989,330.221427243102));
#44589=CARTESIAN_POINT('Ctrl Pts',(166.609736691383,-1.29650859307653,330.255714117954));
#44590=CARTESIAN_POINT('Ctrl Pts',(166.601961612605,-1.42812323760285,330.291681494678));
#44591=CARTESIAN_POINT('Ctrl Pts',(166.594186533826,-1.55844802928339,330.333186681303));
#44592=CARTESIAN_POINT('Ctrl Pts',(166.586411455048,-1.68698153388864,330.380121606923));
#44593=CARTESIAN_POINT('Ctrl Pts',(166.578645943999,-1.81535686983368,330.42699877613));
#44594=CARTESIAN_POINT('Ctrl Pts',(166.57088043295,-1.94194494096252,330.479292256995));
#44595=CARTESIAN_POINT('Ctrl Pts',(166.563114921901,-2.06625681474186,330.536843511814));
#44596=CARTESIAN_POINT('Ctrl Pts',(166.555357110379,-2.19044543293661,330.594337704397));
#44597=CARTESIAN_POINT('Ctrl Pts',(166.547599298856,-2.31236199263233,330.657079133417));
#44598=CARTESIAN_POINT('Ctrl Pts',(166.539841487334,-2.43153532304733,330.724860349033));
#44599=CARTESIAN_POINT('Ctrl Pts',(166.532089513811,-2.55061897175201,330.792590557134));
#44600=CARTESIAN_POINT('Ctrl Pts',(166.524337540288,-2.66696316180209,330.865352810382));
#44601=CARTESIAN_POINT('Ctrl Pts',(166.516585566765,-2.7801195474,330.942892857631));
#44602=CARTESIAN_POINT('Ctrl Pts',(166.508836876208,-2.89322801120153,331.020400066624));
#44603=CARTESIAN_POINT('Ctrl Pts',(166.50108818565,-3.00315103391497,331.102680824733));
#44604=CARTESIAN_POINT('Ctrl Pts',(166.493339495092,-3.10946778975002,331.189436639156));
#44605=CARTESIAN_POINT('Ctrl Pts',(166.485592416715,-3.21576242549584,331.276174403307));
#44606=CARTESIAN_POINT('Ctrl Pts',(166.477845338337,-3.31845198413921,331.367385124834));
#44607=CARTESIAN_POINT('Ctrl Pts',(166.470098259959,-3.41714770359287,331.462729211054));
#44608=CARTESIAN_POINT('Ctrl Pts',(166.462351116653,-3.51584425021167,331.55807409635));
#44609=CARTESIAN_POINT('Ctrl Pts',(166.454603973347,-3.61054660975593,331.657552143858));
#44610=CARTESIAN_POINT('Ctrl Pts',(166.446856830042,-3.70090225848921,331.760786278183));
#44611=CARTESIAN_POINT('Ctrl Pts',(166.439107945013,-3.79127822109058,331.864043621732));
#44612=CARTESIAN_POINT('Ctrl Pts',(166.431359059985,-3.87730527091292,331.971058438386));
#44613=CARTESIAN_POINT('Ctrl Pts',(166.423610174957,-3.9586708791634,332.081420219873));
#44614=CARTESIAN_POINT('Ctrl Pts',(166.415853065183,-4.04012284971122,332.191899140496));
#44615=CARTESIAN_POINT('Ctrl Pts',(166.408095955408,-4.11690326286945,332.305731807299));
#44616=CARTESIAN_POINT('Ctrl Pts',(166.400338845633,-4.18874239124351,332.422477887137));
#44617=CARTESIAN_POINT('Ctrl Pts',(166.392577590707,-4.26061990815084,332.539286352346));
#44618=CARTESIAN_POINT('Ctrl Pts',(166.384816335781,-4.32755068827428,332.659010991716));
#44619=CARTESIAN_POINT('Ctrl Pts',(166.377055080855,-4.38931127891853,332.781187353728));
#44620=CARTESIAN_POINT('Ctrl Pts',(166.36928141045,-4.45117066638002,332.903559158101));
#44621=CARTESIAN_POINT('Ctrl Pts',(166.361507740045,-4.50784317555067,333.028390166249));
#44622=CARTESIAN_POINT('Ctrl Pts',(166.353734069641,-4.55915342276538,333.155195639048));
#44623=CARTESIAN_POINT('Ctrl Pts',(166.346322265464,-4.60807516562759,333.27609828658));
#44624=CARTESIAN_POINT('Ctrl Pts',(166.338910461287,-4.65212254109825,333.398795442048));
#44625=CARTESIAN_POINT('Ctrl Pts',(166.331498657109,-4.69118640647375,333.522856417874));
#44626=CARTESIAN_POINT('Ctrl Pts',(166.322082044832,-4.74081659981526,333.680474466093));
#44627=CARTESIAN_POINT('Ctrl Pts',(166.312665432554,-4.78253107194937,333.840696708659));
#44628=CARTESIAN_POINT('Ctrl Pts',(166.303248820276,-4.81609572084062,334.002801388789));
#44629=CARTESIAN_POINT('Ctrl Pts',(166.293796724985,-4.84978684566856,334.165516900313));
#44630=CARTESIAN_POINT('Ctrl Pts',(166.284344629695,-4.87526646562748,334.330129101346));
#44631=CARTESIAN_POINT('Ctrl Pts',(166.274892534404,-4.89234628133885,334.495885999034));
#44632=CARTESIAN_POINT('Ctrl Pts',(166.265440439114,-4.90942609705022,334.661642896723));
#44633=CARTESIAN_POINT('Ctrl Pts',(166.255988343823,-4.91810593516986,334.828544509634));
#44634=CARTESIAN_POINT('Ctrl Pts',(166.246536248533,-4.9182482206735,334.995816419961));
#44635=CARTESIAN_POINT('',(169.746536248436,-4.91824799493152,335.004441041773));
#44636=CARTESIAN_POINT('Ctrl Pts',(169.746536248436,-4.91824799493153,335.004441041773));
#44637=CARTESIAN_POINT('Ctrl Pts',(169.736906562874,-4.91809427474665,335.174679024157));
#44638=CARTESIAN_POINT('Ctrl Pts',(169.727276877313,-4.90909813996316,335.344523781032));
#44639=CARTESIAN_POINT('Ctrl Pts',(169.717647191752,-4.89140358538227,335.513180306919));
#44640=CARTESIAN_POINT('Ctrl Pts',(169.707853191742,-4.87340710287746,335.68471467381));
#44641=CARTESIAN_POINT('Ctrl Pts',(169.698059191733,-4.84641285341689,335.855020025711));
#44642=CARTESIAN_POINT('Ctrl Pts',(169.688265191723,-4.81062090901127,336.023283700781));
#44643=CARTESIAN_POINT('Ctrl Pts',(169.682295150614,-4.78880353314214,336.125850686315));
#44644=CARTESIAN_POINT('Ctrl Pts',(169.676325109505,-4.76371818085054,336.227659510964));
#44645=CARTESIAN_POINT('Ctrl Pts',(169.670355068397,-4.73541877841011,336.328530035634));
#44646=CARTESIAN_POINT('Ctrl Pts',(169.662579989618,-4.69856307183378,336.459898691465));
#44647=CARTESIAN_POINT('Ctrl Pts',(169.65480491084,-4.65617839560353,336.589940112037));
#44648=CARTESIAN_POINT('Ctrl Pts',(169.647029832061,-4.60837620570426,336.718153604658));
#44649=CARTESIAN_POINT('Ctrl Pts',(169.639264321012,-4.56063283944293,336.846209322414));
#44650=CARTESIAN_POINT('Ctrl Pts',(169.631498809963,-4.50748535936967,336.972441225097));
#44651=CARTESIAN_POINT('Ctrl Pts',(169.623733298914,-4.44909560265916,337.096361462367));
#44652=CARTESIAN_POINT('Ctrl Pts',(169.615975487392,-4.39076373956246,337.220158832362));
#44653=CARTESIAN_POINT('Ctrl Pts',(169.60821767587,-4.32720010914372,337.341648746887));
#44654=CARTESIAN_POINT('Ctrl Pts',(169.600459864348,-4.25861533960452,337.460361447386));
#44655=CARTESIAN_POINT('Ctrl Pts',(169.592707890825,-4.1900821822793,337.578984812814));
#44656=CARTESIAN_POINT('Ctrl Pts',(169.584955917302,-4.11653560163343,337.694834787053));
#44657=CARTESIAN_POINT('Ctrl Pts',(169.577203943779,-4.03823287190434,337.807464752187));
#44658=CARTESIAN_POINT('Ctrl Pts',(169.569455253221,-3.95996330342776,337.920047018463));
#44659=CARTESIAN_POINT('Ctrl Pts',(169.561706562663,-3.87694181469024,338.02941166762));
#44660=CARTESIAN_POINT('Ctrl Pts',(169.553957872106,-3.78946973466079,338.135139900003));
#44661=CARTESIAN_POINT('Ctrl Pts',(169.546210793728,-3.70201585392821,338.240846134744));
#44662=CARTESIAN_POINT('Ctrl Pts',(169.53846371535,-3.61011347275525,338.342917156638));
#44663=CARTESIAN_POINT('Ctrl Pts',(169.530716636972,-3.51410480244014,338.440966506662));
#44664=CARTESIAN_POINT('Ctrl Pts',(169.522969493666,-3.4180953274799,338.539016678433));
#44665=CARTESIAN_POINT('Ctrl Pts',(169.51522235036,-3.31797976820315,338.633044831824));
#44666=CARTESIAN_POINT('Ctrl Pts',(169.507475207055,-3.21413757295082,338.722700998555));
#44667=CARTESIAN_POINT('Ctrl Pts',(169.499726322027,-3.11027203176837,338.812377321897));
#44668=CARTESIAN_POINT('Ctrl Pts',(169.491977436998,-3.00267848322954,338.897679447295));
#44669=CARTESIAN_POINT('Ctrl Pts',(169.48422855197,-2.89176953759251,338.978297626366));
#44670=CARTESIAN_POINT('Ctrl Pts',(169.476471442196,-2.78074287205469,339.059001374405));
#44671=CARTESIAN_POINT('Ctrl Pts',(169.468714332421,-2.66639409656422,339.135011014717));
#44672=CARTESIAN_POINT('Ctrl Pts',(169.460957222646,-2.54916535642159,339.206059800825));
#44673=CARTESIAN_POINT('Ctrl Pts',(169.45319596772,-2.43187397298848,339.277146553134));
#44674=CARTESIAN_POINT('Ctrl Pts',(169.445434712794,-2.31169990067159,339.34326698071));
#44675=CARTESIAN_POINT('Ctrl Pts',(169.437673457867,-2.18910908997195,339.404200773659));
#44676=CARTESIAN_POINT('Ctrl Pts',(169.429899787463,-2.06632217392745,339.465232040819));
#44677=CARTESIAN_POINT('Ctrl Pts',(169.422126117058,-1.94111115128372,339.521059934381));
#44678=CARTESIAN_POINT('Ctrl Pts',(169.414352446653,-1.813961934944,339.571512349439));
#44679=CARTESIAN_POINT('Ctrl Pts',(169.406940642476,-1.69273154521676,339.619616192438));
#44680=CARTESIAN_POINT('Ctrl Pts',(169.399528838299,-1.56973961832718,339.6628336561));
#44681=CARTESIAN_POINT('Ctrl Pts',(169.392117034122,-1.4454175693604,339.701058509813));
#44682=CARTESIAN_POINT('Ctrl Pts',(169.384341955344,-1.31500212643597,339.741156877473));
#44683=CARTESIAN_POINT('Ctrl Pts',(169.376566876566,-1.18271074122502,339.77588757344));
#44684=CARTESIAN_POINT('Ctrl Pts',(169.368791797787,-1.04902477212184,339.805073369885));
#44685=CARTESIAN_POINT('Ctrl Pts',(169.361026286738,-0.915503312114484,
339.834223251349));
#44686=CARTESIAN_POINT('Ctrl Pts',(169.353260775689,-0.780591061039154,
339.85784172723));
#44687=CARTESIAN_POINT('Ctrl Pts',(169.34549526464,-0.644785842036669,339.87580088605));
#44688=CARTESIAN_POINT('Ctrl Pts',(169.337737453118,-0.509115274304072,
339.893742238312));
#44689=CARTESIAN_POINT('Ctrl Pts',(169.329979641596,-0.37255388560567,339.906035389262));
#44690=CARTESIAN_POINT('Ctrl Pts',(169.322221830073,-0.235610688940603,
339.912603247338));
#44691=CARTESIAN_POINT('Ctrl Pts',(169.31446985655,-0.0987705463739764,
339.919166162893));
#44692=CARTESIAN_POINT('Ctrl Pts',(169.306717883027,0.0384504434042439,
339.920012342711));
#44693=CARTESIAN_POINT('Ctrl Pts',(169.298965909504,0.175537484005724,339.915116443606));
#44694=CARTESIAN_POINT('Ctrl Pts',(169.291217218947,0.312566468164167,339.910222617917));
#44695=CARTESIAN_POINT('Ctrl Pts',(169.283468528389,0.449461226160686,339.899591563854));
#44696=CARTESIAN_POINT('Ctrl Pts',(169.275719837832,0.585706514034807,339.883250038849));
#44697=CARTESIAN_POINT('Ctrl Pts',(169.267972759454,0.721923454938865,339.866911913835));
#44698=CARTESIAN_POINT('Ctrl Pts',(169.260225681076,0.85749080665001,339.844865727636));
#44699=CARTESIAN_POINT('Ctrl Pts',(169.252478602698,0.99189839735956,339.817190117882));
#44700=CARTESIAN_POINT('Ctrl Pts',(169.244731459392,1.12630711453411,339.789514276178));
#44701=CARTESIAN_POINT('Ctrl Pts',(169.236984316087,1.25955566847734,339.756208995645));
#44702=CARTESIAN_POINT('Ctrl Pts',(169.229237172781,1.39114442212714,339.71740397457));
#44703=CARTESIAN_POINT('Ctrl Pts',(169.221488287753,1.52276275972243,339.678590229302));
#44704=CARTESIAN_POINT('Ctrl Pts',(169.213739402725,1.65272017964195,339.634274393616));
#44705=CARTESIAN_POINT('Ctrl Pts',(169.205990517697,1.78053292077407,339.584635817657));
#44706=CARTESIAN_POINT('Ctrl Pts',(169.198233407922,1.90848132367025,339.5349445548));
#44707=CARTESIAN_POINT('Ctrl Pts',(169.190476298147,2.03428013555196,339.479919407771));
#44708=CARTESIAN_POINT('Ctrl Pts',(169.182719188372,2.15746577342481,339.419787834161));
#44709=CARTESIAN_POINT('Ctrl Pts',(169.174957933446,2.28071723776381,339.359624128162));
#44710=CARTESIAN_POINT('Ctrl Pts',(169.16719667852,2.40135240204773,339.2943487443));
#44711=CARTESIAN_POINT('Ctrl Pts',(169.159435423594,2.51893385043307,339.224234287968));
#44712=CARTESIAN_POINT('Ctrl Pts',(169.151661753189,2.63670339081611,339.154007671356));
#44713=CARTESIAN_POINT('Ctrl Pts',(169.143888082785,2.7514091265073,339.078926727765));
#44714=CARTESIAN_POINT('Ctrl Pts',(169.13611441238,2.86264337546678,338.999306935882));
#44715=CARTESIAN_POINT('Ctrl Pts',(169.128702608203,2.96869964337571,338.923393464467));
#44716=CARTESIAN_POINT('Ctrl Pts',(169.121290804026,3.07160011948947,338.843354378633));
#44717=CARTESIAN_POINT('Ctrl Pts',(169.113878999849,3.17102200876316,338.759494977047));
#44718=CARTESIAN_POINT('Ctrl Pts',(169.10610392107,3.27531686099277,338.671525376385));
#44719=CARTESIAN_POINT('Ctrl Pts',(169.098328842292,3.37611310359405,338.579073500683));
#44720=CARTESIAN_POINT('Ctrl Pts',(169.090553763514,3.47300121125691,338.482448226336));
#44721=CARTESIAN_POINT('Ctrl Pts',(169.082788252465,3.56977009193509,338.38594185554));
#44722=CARTESIAN_POINT('Ctrl Pts',(169.075022741416,3.66264013250227,338.285272577912));
#44723=CARTESIAN_POINT('Ctrl Pts',(169.067257230367,3.75123436879995,338.180789803309));
#44724=CARTESIAN_POINT('Ctrl Pts',(169.059499418844,3.83974076365441,338.076410623682));
#44725=CARTESIAN_POINT('Ctrl Pts',(169.051741607322,3.92397953986661,337.968225767876));
#44726=CARTESIAN_POINT('Ctrl Pts',(169.0439837958,4.00361041335615,337.856621557114));
#44727=CARTESIAN_POINT('Ctrl Pts',(169.036231822277,4.08318136208807,337.74510133206));
#44728=CARTESIAN_POINT('Ctrl Pts',(169.028479848754,4.15815108405777,337.630167190727));
#44729=CARTESIAN_POINT('Ctrl Pts',(169.020727875231,4.22821968177318,337.512238321729));
#44730=CARTESIAN_POINT('Ctrl Pts',(169.012979184673,4.29825860539588,337.394359395678));
#44731=CARTESIAN_POINT('Ctrl Pts',(169.005230494116,4.36340033380143,337.273488599793));
#44732=CARTESIAN_POINT('Ctrl Pts',(168.997481803558,4.42338853981542,337.150073693697));
#44733=CARTESIAN_POINT('Ctrl Pts',(168.98973472518,4.48336426478213,337.026684465104));
#44734=CARTESIAN_POINT('Ctrl Pts',(168.981987646802,4.53818842933706,336.900752530485));
#44735=CARTESIAN_POINT('Ctrl Pts',(168.974240568425,4.58765107829978,336.772749459533));
#44736=CARTESIAN_POINT('Ctrl Pts',(168.966493425119,4.63711414180711,336.644745315792));
#44737=CARTESIAN_POINT('Ctrl Pts',(168.958746281813,4.68121545920871,336.514670365694));
#44738=CARTESIAN_POINT('Ctrl Pts',(168.950999138507,4.71979371427856,336.383014951892));
#44739=CARTESIAN_POINT('Ctrl Pts',(168.943250253479,4.75838064255917,336.251329939157));
#44740=CARTESIAN_POINT('Ctrl Pts',(168.935501368451,4.79144192776782,336.118064130695));
#44741=CARTESIAN_POINT('Ctrl Pts',(168.927752483423,4.81886659837128,335.9837213882));
#44742=CARTESIAN_POINT('Ctrl Pts',(168.919995373648,4.84632037780348,335.849236052929));
#44743=CARTESIAN_POINT('Ctrl Pts',(168.912238263874,4.86812551320016,335.713671883818));
#44744=CARTESIAN_POINT('Ctrl Pts',(168.904481154099,4.88422240714451,335.577541808052));
#44745=CARTESIAN_POINT('Ctrl Pts',(168.896719899173,4.90032790275431,335.441338988725));
#44746=CARTESIAN_POINT('Ctrl Pts',(168.888958644246,4.9107190493142,335.304570049732));
#44747=CARTESIAN_POINT('Ctrl Pts',(168.88119738932,4.91538837570153,335.167750345807));
#44748=CARTESIAN_POINT('Ctrl Pts',(168.873423718916,4.92006517148935,335.030711774945));
#44749=CARTESIAN_POINT('Ctrl Pts',(168.865650048511,4.9190018596383,334.893622667941));
#44750=CARTESIAN_POINT('Ctrl Pts',(168.857876378106,4.91224311276248,334.756996576943));
#44751=CARTESIAN_POINT('Ctrl Pts',(168.850464573929,4.90579898717977,334.62673046335));
#44752=CARTESIAN_POINT('Ctrl Pts',(168.843052769752,4.89417776439534,334.496885515713));
#44753=CARTESIAN_POINT('Ctrl Pts',(168.835640965575,4.8774614936528,334.3678983939));
#44754=CARTESIAN_POINT('Ctrl Pts',(168.827865886797,4.85992590868598,334.232589229014));
#44755=CARTESIAN_POINT('Ctrl Pts',(168.820090808018,4.83672778459249,334.097796503387));
#44756=CARTESIAN_POINT('Ctrl Pts',(168.81231572924,4.80790524447894,333.96403174633));
#44757=CARTESIAN_POINT('Ctrl Pts',(168.804550218191,4.77911817233594,333.830431595322));
#44758=CARTESIAN_POINT('Ctrl Pts',(168.796784707142,4.74472053692603,333.697857274387));
#44759=CARTESIAN_POINT('Ctrl Pts',(168.789019196093,4.70480216751732,333.566814866452));
#44760=CARTESIAN_POINT('Ctrl Pts',(168.78126138457,4.6649233772881,333.435902387445));
#44761=CARTESIAN_POINT('Ctrl Pts',(168.773503573048,4.61953485944662,333.30651917025));
#44762=CARTESIAN_POINT('Ctrl Pts',(168.765745761526,4.56877733250919,333.179160427591));
#44763=CARTESIAN_POINT('Ctrl Pts',(168.757993788003,4.51805800222039,333.051897526425));
#44764=CARTESIAN_POINT('Ctrl Pts',(168.75024181448,4.46197784908123,332.926656429017));
#44765=CARTESIAN_POINT('Ctrl Pts',(168.742489840957,4.40072708599791,332.803916172578));
#44766=CARTESIAN_POINT('Ctrl Pts',(168.734741150399,4.33950226264913,332.681227896711));
#44767=CARTESIAN_POINT('Ctrl Pts',(168.726992459842,4.27311135879626,332.561038704339));
#44768=CARTESIAN_POINT('Ctrl Pts',(168.719243769284,4.20179219171555,332.443806454875));
#44769=CARTESIAN_POINT('Ctrl Pts',(168.711496690906,4.1304878631832,332.32659859656));
#44770=CARTESIAN_POINT('Ctrl Pts',(168.703749612528,4.0542575139732,332.212346791169));
#44771=CARTESIAN_POINT('Ctrl Pts',(168.696002534151,3.97338407830348,332.10148278791));
#44772=CARTESIAN_POINT('Ctrl Pts',(168.688255390845,3.89250996483651,331.990617855503));
#44773=CARTESIAN_POINT('Ctrl Pts',(168.680508247539,3.80699291765138,331.883141097643));
#44774=CARTESIAN_POINT('Ctrl Pts',(168.672761104233,3.71715797887775,331.779453521129));
#44775=CARTESIAN_POINT('Ctrl Pts',(168.665012219205,3.62730284330266,331.675742633447));
#44776=CARTESIAN_POINT('Ctrl Pts',(168.657263334177,3.53312814034821,331.575822917634));
#44777=CARTESIAN_POINT('Ctrl Pts',(168.649514449149,3.43499752499764,331.480060360495));
#44778=CARTESIAN_POINT('Ctrl Pts',(168.641757339374,3.33676275279803,331.384196159988));
#44779=CARTESIAN_POINT('Ctrl Pts',(168.634000229599,3.23456396079939,331.292498205864));
#44780=CARTESIAN_POINT('Ctrl Pts',(168.626243119825,3.12880022883224,331.205294189195));
#44781=CARTESIAN_POINT('Ctrl Pts',(168.618481864899,3.02297998010843,331.118043573487));
#44782=CARTESIAN_POINT('Ctrl Pts',(168.610720609972,2.91359130711932,331.03529191597));
#44783=CARTESIAN_POINT('Ctrl Pts',(168.602959355046,2.80106353960211,330.957324387289));
#44784=CARTESIAN_POINT('Ctrl Pts',(168.595185684642,2.68835576432956,330.87923213597));
#44785=CARTESIAN_POINT('Ctrl Pts',(168.587412014237,2.57249919052745,330.80593951562));
#44786=CARTESIAN_POINT('Ctrl Pts',(168.579638343832,2.45394985006524,330.737686872617));
#44787=CARTESIAN_POINT('Ctrl Pts',(168.572226539655,2.34091900992311,330.672611406566));
#44788=CARTESIAN_POINT('Ctrl Pts',(168.564814735478,2.22544071286094,330.612117389065));
#44789=CARTESIAN_POINT('Ctrl Pts',(168.557402931301,2.107926557031,330.556372124867));
#44790=CARTESIAN_POINT('Ctrl Pts',(168.549627852523,1.984652682367,330.497894619213));
#44791=CARTESIAN_POINT('Ctrl Pts',(168.541852773744,1.8587487676556,330.444458338431));
#44792=CARTESIAN_POINT('Ctrl Pts',(168.534077694966,1.73066559940786,330.396308041851));
#44793=CARTESIAN_POINT('Ctrl Pts',(168.526312183917,1.60274004565279,330.348216997276));
#44794=CARTESIAN_POINT('Ctrl Pts',(168.518546672868,1.47264093657317,330.305399130563));
#44795=CARTESIAN_POINT('Ctrl Pts',(168.510781161819,1.34084245987025,330.268052772874));
#44796=CARTESIAN_POINT('Ctrl Pts',(168.503023350296,1.20917466174083,330.230743444207));
#44797=CARTESIAN_POINT('Ctrl Pts',(168.495265538774,1.07581122273547,330.19889493435));
#44798=CARTESIAN_POINT('Ctrl Pts',(168.487507727252,0.941244728661796,330.17265689812));
#44799=CARTESIAN_POINT('Ctrl Pts',(168.479755753729,0.806779500142261,330.146438606845));
#44800=CARTESIAN_POINT('Ctrl Pts',(168.472003780206,0.6711134006884,330.125822459897));
#44801=CARTESIAN_POINT('Ctrl Pts',(168.464251806683,0.534752198028195,330.110907737708));
#44802=CARTESIAN_POINT('Ctrl Pts',(168.456503116125,0.398448744418182,330.095999331913));
#44803=CARTESIAN_POINT('Ctrl Pts',(168.448754425568,0.261451160844527,330.086787590903));
#44804=CARTESIAN_POINT('Ctrl Pts',(168.44100573501,0.124273167629879,330.083320303059));
#44805=CARTESIAN_POINT('Ctrl Pts',(168.433258656632,-0.012876284557547,
330.079853736614));
#44806=CARTESIAN_POINT('Ctrl Pts',(168.425511578255,-0.150205681220574,
330.082129255903));
#44807=CARTESIAN_POINT('Ctrl Pts',(168.417764499877,-0.287198843298569,
330.090142579778));
#44808=CARTESIAN_POINT('Ctrl Pts',(168.410017356571,-0.42419315351114,330.098155970813));
#44809=CARTESIAN_POINT('Ctrl Pts',(168.402270213265,-0.560850833310727,
330.111907239524));
#44810=CARTESIAN_POINT('Ctrl Pts',(168.394523069959,-0.696658768576774,
330.131340058839));
#44811=CARTESIAN_POINT('Ctrl Pts',(168.386774184931,-0.832497236349791,
330.150777247065));
#44812=CARTESIAN_POINT('Ctrl Pts',(168.379025299903,-0.967485192582247,
330.17589847229));
#44813=CARTESIAN_POINT('Ctrl Pts',(168.371276414875,-1.10111807658499,330.206595985741));
#44814=CARTESIAN_POINT('Ctrl Pts',(168.3635193051,-1.23489279991167,330.237326081849));
#44815=CARTESIAN_POINT('Ctrl Pts',(168.355762195326,-1.36730919634014,330.273644201753));
#44816=CARTESIAN_POINT('Ctrl Pts',(168.348005085551,-1.49787573846262,330.315392083149));
#44817=CARTESIAN_POINT('Ctrl Pts',(168.340243830625,-1.62851205117045,330.357162273278));
#44818=CARTESIAN_POINT('Ctrl Pts',(168.332482575698,-1.75729617308055,330.404367871928));
#44819=CARTESIAN_POINT('Ctrl Pts',(168.324721320772,-1.88375596315883,330.456802168762));
#44820=CARTESIAN_POINT('Ctrl Pts',(168.316947650368,-2.01041804768812,330.509320343383));
#44821=CARTESIAN_POINT('Ctrl Pts',(168.309173979963,-2.13474801570329,330.567083765584));
#44822=CARTESIAN_POINT('Ctrl Pts',(168.301400309558,-2.25629696979506,330.629839013653));
#44823=CARTESIAN_POINT('Ctrl Pts',(168.293988505381,-2.37218779083118,330.689672989826));
#44824=CARTESIAN_POINT('Ctrl Pts',(168.286576701204,-2.48555043341456,330.754044369432));
#44825=CARTESIAN_POINT('Ctrl Pts',(168.279164897027,-2.59602146803341,330.822697569003));
#44826=CARTESIAN_POINT('Ctrl Pts',(168.271389818249,-2.71190701713495,330.894715666393));
#44827=CARTESIAN_POINT('Ctrl Pts',(168.26361473947,-2.82497655827244,330.971673516613));
#44828=CARTESIAN_POINT('Ctrl Pts',(168.255839660692,-2.93478032165797,331.053324496984));
#44829=CARTESIAN_POINT('Ctrl Pts',(168.248074149643,-3.04444896452226,331.134875000625));
#44830=CARTESIAN_POINT('Ctrl Pts',(168.240308638594,-3.15085951512902,331.221106912426));
#44831=CARTESIAN_POINT('Ctrl Pts',(168.232543127545,-3.25358858239829,331.311728806204));
#44832=CARTESIAN_POINT('Ctrl Pts',(168.224785316022,-3.35621579349819,331.40226084811));
#44833=CARTESIAN_POINT('Ctrl Pts',(168.2170275045,-3.45516849413348,331.497173953003));
#44834=CARTESIAN_POINT('Ctrl Pts',(168.209269692978,-3.55005426993032,331.596134881778));
#44835=CARTESIAN_POINT('Ctrl Pts',(168.201517719455,-3.64486864117196,331.695021339316));
#44836=CARTESIAN_POINT('Ctrl Pts',(168.193765745932,-3.73562190990028,331.797949276588));
#44837=CARTESIAN_POINT('Ctrl Pts',(168.186013772409,-3.82195688914436,331.904547109061));
#44838=CARTESIAN_POINT('Ctrl Pts',(168.178265081851,-3.90825530547336,332.011099797289));
#44839=CARTESIAN_POINT('Ctrl Pts',(168.170516391294,-3.99013890840325,332.121318986401));
#44840=CARTESIAN_POINT('Ctrl Pts',(168.162767700736,-4.06728950812258,332.234798539054));
#44841=CARTESIAN_POINT('Ctrl Pts',(168.155020622358,-4.14442405601523,332.348254481339));
#44842=CARTESIAN_POINT('Ctrl Pts',(168.14727354398,-4.21682733979214,332.464969114844));
#44843=CARTESIAN_POINT('Ctrl Pts',(168.139526465603,-4.28422362545514,332.584506056809));
#44844=CARTESIAN_POINT('Ctrl Pts',(168.131779322297,-4.3516204759639,332.704044000609));
#44845=CARTESIAN_POINT('Ctrl Pts',(168.124032178991,-4.41401005268988,332.826403959564));
#44846=CARTESIAN_POINT('Ctrl Pts',(168.116285035685,-4.4711620467765,332.951123963251));
#44847=CARTESIAN_POINT('Ctrl Pts',(168.108536150657,-4.52832688984473,333.075872006642));
#44848=CARTESIAN_POINT('Ctrl Pts',(168.100787265629,-4.58025164433972,333.202980795305));
#44849=CARTESIAN_POINT('Ctrl Pts',(168.093038380601,-4.62675387176355,333.331967724347));
#44850=CARTESIAN_POINT('Ctrl Pts',(168.085281270826,-4.67330545713206,333.461091561448));
#44851=CARTESIAN_POINT('Ctrl Pts',(168.077524161051,-4.71442288545073,333.592097152797));
#44852=CARTESIAN_POINT('Ctrl Pts',(168.069767051276,-4.74997324918173,333.7244855177));
#44853=CARTESIAN_POINT('Ctrl Pts',(168.06200579635,-4.78554260989044,333.856944626711));
#44854=CARTESIAN_POINT('Ctrl Pts',(168.054244541424,-4.81553889289518,333.990787600401));
#44855=CARTESIAN_POINT('Ctrl Pts',(168.046483286498,-4.83988042272313,334.125505542475));
#44856=CARTESIAN_POINT('Ctrl Pts',(168.038709616093,-4.86426089106589,334.260438989353));
#44857=CARTESIAN_POINT('Ctrl Pts',(168.030935945688,-4.88296847675385,334.396249814137));
#44858=CARTESIAN_POINT('Ctrl Pts',(168.023162275284,-4.89597336336474,334.532423388392));
#44859=CARTESIAN_POINT('Ctrl Pts',(168.015750471107,-4.90837286937501,334.662258050002));
#44860=CARTESIAN_POINT('Ctrl Pts',(168.00833866693,-4.91558863361006,334.792422161769));
#44861=CARTESIAN_POINT('Ctrl Pts',(168.000926862752,-4.91763890909733,334.922471797183));
#44862=CARTESIAN_POINT('Ctrl Pts',(167.999463324665,-4.91804375738991,334.948151454953));
#44863=CARTESIAN_POINT('Ctrl Pts',(167.997999786577,-4.91824746069164,334.973834292198));
#44864=CARTESIAN_POINT('Ctrl Pts',(167.99653624849,-4.91824997640721,334.999518263041));
#44865=CARTESIAN_POINT('',(171.496536248527,-4.91824971188752,334.998316545704));
#44866=CARTESIAN_POINT('Ctrl Pts',(171.49653624849,-4.91824971188774,334.998316546354));
#44867=CARTESIAN_POINT('Ctrl Pts',(171.488603707819,-4.91829790514505,335.139114289432));
#44868=CARTESIAN_POINT('Ctrl Pts',(171.480671167148,-4.91229569124257,335.279865940706));
#44869=CARTESIAN_POINT('Ctrl Pts',(171.472738626477,-4.90028124430733,335.420031890682));
#44870=CARTESIAN_POINT('Ctrl Pts',(171.464801568283,-4.88825995523447,335.560277664117));
#44871=CARTESIAN_POINT('Ctrl Pts',(171.456864510089,-4.87021964015133,335.699936708887));
#44872=CARTESIAN_POINT('Ctrl Pts',(171.448927451896,-4.84625020104069,335.838476029123));
#44873=CARTESIAN_POINT('Ctrl Pts',(171.440984525747,-4.8222630410576,335.977117773016));
#44874=CARTESIAN_POINT('Ctrl Pts',(171.433041599598,-4.7923380824285,336.114637784287));
#44875=CARTESIAN_POINT('Ctrl Pts',(171.425098673449,-4.75661600854616,336.250514777898));
#44876=CARTESIAN_POINT('Ctrl Pts',(171.417142776465,-4.72083560035479,336.386613659258));
#44877=CARTESIAN_POINT('Ctrl Pts',(171.409186879482,-4.67923925564794,336.521063810024));
#44878=CARTESIAN_POINT('Ctrl Pts',(171.401230982498,-4.63201741025085,336.65335954155));
#44879=CARTESIAN_POINT('Ctrl Pts',(171.393267950449,-4.58475321500933,336.785773919511));
#44880=CARTESIAN_POINT('Ctrl Pts',(171.385304918399,-4.53185359555243,336.916029689037));
#44881=CARTESIAN_POINT('Ctrl Pts',(171.377341886349,-4.47355635531153,337.04364297233));
#44882=CARTESIAN_POINT('Ctrl Pts',(171.369364296103,-4.41515253473246,337.171489561124));
#44883=CARTESIAN_POINT('Ctrl Pts',(171.361386705857,-4.35133153930368,337.296683686043));
#44884=CARTESIAN_POINT('Ctrl Pts',(171.353409115612,-4.28237670327676,337.418766800196));
#44885=CARTESIAN_POINT('Ctrl Pts',(171.348867168421,-4.2431180782887,337.488273385551));
#44886=CARTESIAN_POINT('Ctrl Pts',(171.34432522123,-4.20219613096733,337.556772086059));
#44887=CARTESIAN_POINT('Ctrl Pts',(171.33978327404,-4.15966913126676,337.624182878705));
#44888=CARTESIAN_POINT('Ctrl Pts',(171.332008195261,-4.08686978794295,337.739579249765));
#44889=CARTESIAN_POINT('Ctrl Pts',(171.324233116483,-4.00914982865405,337.852126305575));
#44890=CARTESIAN_POINT('Ctrl Pts',(171.316458037705,-3.92675890896485,337.961375952723));
#44891=CARTESIAN_POINT('Ctrl Pts',(171.308692526655,-3.84446937654756,338.070491161225));
#44892=CARTESIAN_POINT('Ctrl Pts',(171.300927015606,-3.75752055353427,338.176316725574));
#44893=CARTESIAN_POINT('Ctrl Pts',(171.293161504557,-3.66620671976475,338.278431233144));
#44894=CARTESIAN_POINT('Ctrl Pts',(171.285403693035,-3.57498342392752,338.380444493881));
#44895=CARTESIAN_POINT('Ctrl Pts',(171.277645881513,-3.47940398901383,338.478753730808));
#44896=CARTESIAN_POINT('Ctrl Pts',(171.269888069991,-3.3798042975632,338.57296878977));
#44897=CARTESIAN_POINT('Ctrl Pts',(171.262136096468,-3.2802795580389,338.667112948914));
#44898=CARTESIAN_POINT('Ctrl Pts',(171.254384122945,-3.17674086664551,338.757168795145));
#44899=CARTESIAN_POINT('Ctrl Pts',(171.246632149422,-3.06956221249043,338.842781659963));
#44900=CARTESIAN_POINT('Ctrl Pts',(171.238883458864,-2.9624289485588,338.928358267683));
#44901=CARTESIAN_POINT('Ctrl Pts',(171.231134768307,-2.85165909261949,339.009495392925));
#44902=CARTESIAN_POINT('Ctrl Pts',(171.223386077749,-2.7376609223481,339.085877596888));
#44903=CARTESIAN_POINT('Ctrl Pts',(171.215638999371,-2.62368647034811,339.162243908895));
#44904=CARTESIAN_POINT('Ctrl Pts',(171.207891920993,-2.50648536454885,339.233857049974));
#44905=CARTESIAN_POINT('Ctrl Pts',(171.200144842615,-2.38649584053138,339.300444240497));
#44906=CARTESIAN_POINT('Ctrl Pts',(171.19239769931,-2.26650531088626,339.367031989085));
#44907=CARTESIAN_POINT('Ctrl Pts',(171.184650556004,-2.1437266581851,339.428593513435));
#44908=CARTESIAN_POINT('Ctrl Pts',(171.176903412698,-2.01862339820749,339.484901630884));
#44909=CARTESIAN_POINT('Ctrl Pts',(171.16915452767,-1.89349201236096,339.541222407595));
#44910=CARTESIAN_POINT('Ctrl Pts',(171.161405642642,-1.76603533564503,339.592287266795));
#44911=CARTESIAN_POINT('Ctrl Pts',(171.153656757614,-1.63673719444059,339.637917034492));
#44912=CARTESIAN_POINT('Ctrl Pts',(171.145899647839,-1.50730181485311,339.683595234096));
#44913=CARTESIAN_POINT('Ctrl Pts',(171.138142538064,-1.37602143555847,339.723826688068));
#44914=CARTESIAN_POINT('Ctrl Pts',(171.13038542829,-1.24339592375126,339.758481862874));
#44915=CARTESIAN_POINT('Ctrl Pts',(171.122624173363,-1.1106995411112,339.793155556297));
#44916=CARTESIAN_POINT('Ctrl Pts',(171.114862918437,-0.976656975481078,
339.822246950202));
#44917=CARTESIAN_POINT('Ctrl Pts',(171.107101663511,-0.841777663316359,
339.845677808939));
#44918=CARTESIAN_POINT('Ctrl Pts',(171.099327993106,-0.706682588209115,
339.869146149413));
#44919=CARTESIAN_POINT('Ctrl Pts',(171.091554322702,-0.570748479577714,
339.886935809376));
#44920=CARTESIAN_POINT('Ctrl Pts',(171.083780652297,-0.434490155547044,
339.899020449767));
#44921=CARTESIAN_POINT('Ctrl Pts',(171.07636884812,-0.304574689282362,339.91054254724));
#44922=CARTESIAN_POINT('Ctrl Pts',(171.068957043943,-0.174364800245908,
339.916878795561));
#44923=CARTESIAN_POINT('Ctrl Pts',(171.061545239766,-0.0443042815042223,
339.91805044638));
#44924=CARTESIAN_POINT('Ctrl Pts',(171.053770160987,0.092130890691618,339.919279523296));
#44925=CARTESIAN_POINT('Ctrl Pts',(171.045995082209,0.228832840549928,339.914828821295));
#44926=CARTESIAN_POINT('Ctrl Pts',(171.038220003431,0.365289653809286,339.904665792011));
#44927=CARTESIAN_POINT('Ctrl Pts',(171.030454492382,0.501578548272557,339.894515268981));
#44928=CARTESIAN_POINT('Ctrl Pts',(171.022688981333,0.637622520277791,339.878666433876));
#44929=CARTESIAN_POINT('Ctrl Pts',(171.014923470284,0.772907943249615,339.857138702339));
#44930=CARTESIAN_POINT('Ctrl Pts',(171.007165658761,0.908059230331103,339.835632315611));
#44931=CARTESIAN_POINT('Ctrl Pts',(170.999407847239,1.04245308157693,339.808458298778));
#44932=CARTESIAN_POINT('Ctrl Pts',(170.991650035717,1.17557964272247,339.775687967834));
#44933=CARTESIAN_POINT('Ctrl Pts',(170.983898062194,1.30860602190894,339.742942297604));
#44934=CARTESIAN_POINT('Ctrl Pts',(170.976146088671,1.44036663122452,339.704608788909));
#44935=CARTESIAN_POINT('Ctrl Pts',(170.968394115148,1.57036083539402,339.660810005692));
#44936=CARTESIAN_POINT('Ctrl Pts',(170.96064542459,1.7002999869407,339.617029771286));
#44937=CARTESIAN_POINT('Ctrl Pts',(170.952896734033,1.82847385156352,339.567788990371));
#44938=CARTESIAN_POINT('Ctrl Pts',(170.945148043475,1.95439622756584,339.51326029032));
#44939=CARTESIAN_POINT('Ctrl Pts',(170.937400965097,2.08029240436603,339.45874293542));
#44940=CARTESIAN_POINT('Ctrl Pts',(170.929653886719,2.2039376658452,339.398940004977));
#44941=CARTESIAN_POINT('Ctrl Pts',(170.921906808342,2.32486547137441,339.33407240393));
#44942=CARTESIAN_POINT('Ctrl Pts',(170.914159665036,2.44579429039497,339.269204259231));
#44943=CARTESIAN_POINT('Ctrl Pts',(170.90641252173,2.56400526359214,339.199271544032));
#44944=CARTESIAN_POINT('Ctrl Pts',(170.898665378424,2.67905651323399,339.124541097067));
#44945=CARTESIAN_POINT('Ctrl Pts',(170.890916493396,2.79413362883978,339.049793849111));
#44946=CARTESIAN_POINT('Ctrl Pts',(170.883167608368,2.90604927959664,338.970246935906));
#44947=CARTESIAN_POINT('Ctrl Pts',(170.87541872334,3.01439096805303,338.886210256049));
#44948=CARTESIAN_POINT('Ctrl Pts',(170.867661613565,3.1228476514967,338.802084378791));
#44949=CARTESIAN_POINT('Ctrl Pts',(170.85990450379,3.22772248554509,338.713459455323));
#44950=CARTESIAN_POINT('Ctrl Pts',(170.852147394016,3.32863603586379,338.620685736604));
#44951=CARTESIAN_POINT('Ctrl Pts',(170.84438613909,3.42960351115714,338.527862442576));
#44952=CARTESIAN_POINT('Ctrl Pts',(170.836624884163,3.52660520855334,338.430886211971));
#44953=CARTESIAN_POINT('Ctrl Pts',(170.828863629237,3.61929965272588,338.330143102973));
#44954=CARTESIAN_POINT('Ctrl Pts',(170.821089958833,3.71214237780011,338.229238837832));
#44955=CARTESIAN_POINT('Ctrl Pts',(170.813316288428,3.80066382846647,338.124555951633));
#44956=CARTESIAN_POINT('Ctrl Pts',(170.805542618023,3.88456325801952,338.016513112344));
#44957=CARTESIAN_POINT('Ctrl Pts',(170.798130813846,3.96455714894188,337.913499693218));
#44958=CARTESIAN_POINT('Ctrl Pts',(170.790719009669,4.04034947773265,337.807432327161));
#44959=CARTESIAN_POINT('Ctrl Pts',(170.783307205492,4.11171795346504,337.698695709719));
#44960=CARTESIAN_POINT('Ctrl Pts',(170.775532126714,4.18658441078877,337.584629586746));
#44961=CARTESIAN_POINT('Ctrl Pts',(170.767757047935,4.25681898954915,337.467265470468));
#44962=CARTESIAN_POINT('Ctrl Pts',(170.759981969157,4.32211729294997,337.347016226719));
#44963=CARTESIAN_POINT('Ctrl Pts',(170.752216458108,4.38733524263126,337.22691495732));
#44964=CARTESIAN_POINT('Ctrl Pts',(170.744450947059,4.44762881852518,337.103935964809));
#44965=CARTESIAN_POINT('Ctrl Pts',(170.73668543601,4.50273639484788,336.978521675649));
#44966=CARTESIAN_POINT('Ctrl Pts',(170.728927624487,4.55778933184837,336.853231735121));
#44967=CARTESIAN_POINT('Ctrl Pts',(170.721169812965,4.6076663457877,336.725511658688));
#44968=CARTESIAN_POINT('Ctrl Pts',(170.713412001443,4.65215149640935,336.595828786855));
#44969=CARTESIAN_POINT('Ctrl Pts',(170.70566002792,4.69660317054424,336.466243505497));
#44970=CARTESIAN_POINT('Ctrl Pts',(170.697908054397,4.73567093139604,336.334698737004));
#44971=CARTESIAN_POINT('Ctrl Pts',(170.690156080874,4.76918692312449,336.201681802641));
#44972=CARTESIAN_POINT('Ctrl Pts',(170.682407390316,4.80268872081063,336.068721201028));
#44973=CARTESIAN_POINT('Ctrl Pts',(170.674658699759,4.83064333039579,335.934290051809));
#44974=CARTESIAN_POINT('Ctrl Pts',(170.666910009201,4.85293280628301,335.798890630939));
#44975=CARTESIAN_POINT('Ctrl Pts',(170.659162930823,4.87521764465859,335.663519381049));
#44976=CARTESIAN_POINT('Ctrl Pts',(170.651415852446,4.89183963035951,335.527180645661));
#44977=CARTESIAN_POINT('Ctrl Pts',(170.643668774068,4.90273205515801,335.390386293082));
#44978=CARTESIAN_POINT('Ctrl Pts',(170.635921630762,4.91362457124555,335.253590794034));
#44979=CARTESIAN_POINT('Ctrl Pts',(170.628174487456,4.91878739962699,335.116340059819));
#44980=CARTESIAN_POINT('Ctrl Pts',(170.62042734415,4.9182058052906,334.979150076599));
#44981=CARTESIAN_POINT('Ctrl Pts',(170.612678459122,4.91762408019946,334.841929250158));
#44982=CARTESIAN_POINT('Ctrl Pts',(170.604929574094,4.91129536416978,334.704769592685));
#44983=CARTESIAN_POINT('Ctrl Pts',(170.597180689066,4.8992570315022,334.568185685999));
#44984=CARTESIAN_POINT('Ctrl Pts',(170.589423579291,4.88720592122396,334.431456807743));
#44985=CARTESIAN_POINT('Ctrl Pts',(170.581666469517,4.86943312277005,334.295305291));
#44986=CARTESIAN_POINT('Ctrl Pts',(170.573909359742,4.84602783595446,334.160239751087));
#44987=CARTESIAN_POINT('Ctrl Pts',(170.566148104816,4.82261004210197,334.025102036468));
#44988=CARTESIAN_POINT('Ctrl Pts',(170.55838684989,4.79355384530654,333.891051836812));
#44989=CARTESIAN_POINT('Ctrl Pts',(170.550625594963,4.7589990982376,333.758585224241));
#44990=CARTESIAN_POINT('Ctrl Pts',(170.542851924559,4.7243890748347,333.62590670826));
#44991=CARTESIAN_POINT('Ctrl Pts',(170.535078254154,4.68426303883409,333.494817215447));
#44992=CARTESIAN_POINT('Ctrl Pts',(170.527304583749,4.63881030576238,333.365796215384));
#44993=CARTESIAN_POINT('Ctrl Pts',(170.519892779572,4.5954734083504,333.242781173914));
#44994=CARTESIAN_POINT('Ctrl Pts',(170.512480975395,4.54729467545668,333.121646649758));
#44995=CARTESIAN_POINT('Ctrl Pts',(170.505069171218,4.49447731139666,333.002787752931));
#44996=CARTESIAN_POINT('Ctrl Pts',(170.49729409244,4.43907121098931,332.878103227509));
#44997=CARTESIAN_POINT('Ctrl Pts',(170.489519013661,4.37838518238395,332.755529014171));
#44998=CARTESIAN_POINT('Ctrl Pts',(170.481743934883,4.3126016866966,332.63554451207));
#44999=CARTESIAN_POINT('Ctrl Pts',(170.473978423834,4.2468991417886,332.515707658538));
#45000=CARTESIAN_POINT('Ctrl Pts',(170.466212912785,4.17611179690491,332.398454514881));
#45001=CARTESIAN_POINT('Ctrl Pts',(170.458447401736,4.10047011717344,332.284244510147));
#45002=CARTESIAN_POINT('Ctrl Pts',(170.450689590214,4.02490343638772,332.170147744965));
#45003=CARTESIAN_POINT('Ctrl Pts',(170.442931778692,3.94449221351208,332.05908843793));
#45004=CARTESIAN_POINT('Ctrl Pts',(170.435173967169,3.85951258748423,331.951501082573));
#45005=CARTESIAN_POINT('Ctrl Pts',(170.427421993646,3.77459691131963,331.843994690113));
#45006=CARTESIAN_POINT('Ctrl Pts',(170.419670020123,3.68511991621315,331.739955354269));
#45007=CARTESIAN_POINT('Ctrl Pts',(170.4119180466,3.59140056458649,331.639787946098));
#45008=CARTESIAN_POINT('Ctrl Pts',(170.404169356043,3.49772090316113,331.539662958884));
#45009=CARTESIAN_POINT('Ctrl Pts',(170.396420665485,3.39980272510159,331.443406922798));
#45010=CARTESIAN_POINT('Ctrl Pts',(170.388671974927,3.29800457784401,331.35139083115));
#45011=CARTESIAN_POINT('Ctrl Pts',(170.38092489655,3.19622761054127,331.259393884217));
#45012=CARTESIAN_POINT('Ctrl Pts',(170.373177818172,3.09057256952619,331.171635388993));
#45013=CARTESIAN_POINT('Ctrl Pts',(170.365430739794,2.9814337961282,331.088448443162));
#45014=CARTESIAN_POINT('Ctrl Pts',(170.357683596488,2.87229410804189,331.005260800143));
#45015=CARTESIAN_POINT('Ctrl Pts',(170.349936453182,2.75967094020464,330.926645019884));
#45016=CARTESIAN_POINT('Ctrl Pts',(170.342189309877,2.64399022242767,330.852892723089));
#45017=CARTESIAN_POINT('Ctrl Pts',(170.334440424849,2.52828349716938,330.779123845212));
#45018=CARTESIAN_POINT('Ctrl Pts',(170.32669153982,2.40951818364181,330.710220836661));
#45019=CARTESIAN_POINT('Ctrl Pts',(170.318942654792,2.28814723005367,330.646430738337));
#45020=CARTESIAN_POINT('Ctrl Pts',(170.311185545018,2.16664745208172,330.582572932544));
#45021=CARTESIAN_POINT('Ctrl Pts',(170.303428435243,2.04253685594054,330.523839059847));
#45022=CARTESIAN_POINT('Ctrl Pts',(170.295671325468,1.91629141823982,330.470429351155));
#45023=CARTESIAN_POINT('Ctrl Pts',(170.287910070542,1.78997851901345,330.416991102021));
#45024=CARTESIAN_POINT('Ctrl Pts',(170.280148815616,1.66152887095638,330.368882822961));
#45025=CARTESIAN_POINT('Ctrl Pts',(170.27238756069,1.53143531400347,330.326255361969));
#45026=CARTESIAN_POINT('Ctrl Pts',(170.264613890285,1.40113364975705,330.283559710932));
#45027=CARTESIAN_POINT('Ctrl Pts',(170.25684021988,1.26918319806779,330.246362504182));
#45028=CARTESIAN_POINT('Ctrl Pts',(170.249066549476,1.13608960462986,330.214764010756));
#45029=CARTESIAN_POINT('Ctrl Pts',(170.241654745299,1.00919154998876,330.184636434802));
#45030=CARTESIAN_POINT('Ctrl Pts',(170.234242941122,0.881254667472015,330.159598117423));
#45031=CARTESIAN_POINT('Ctrl Pts',(170.226831136945,0.752721179036315,330.139691996475));
#45032=CARTESIAN_POINT('Ctrl Pts',(170.219056058166,0.617887881449027,330.118810217242));
#45033=CARTESIAN_POINT('Ctrl Pts',(170.211280979388,0.481971918204775,330.103510453232));
#45034=CARTESIAN_POINT('Ctrl Pts',(170.203505900609,0.345475166458746,330.093898699389));
#45035=CARTESIAN_POINT('Ctrl Pts',(170.19574038956,0.209146382655525,330.084298773421));
#45036=CARTESIAN_POINT('Ctrl Pts',(170.187974878511,0.0722386185744949,
330.080372957898));
#45037=CARTESIAN_POINT('Ctrl Pts',(170.180209367462,-0.0647370641909145,
330.082176073199));
#45038=CARTESIAN_POINT('Ctrl Pts',(170.17245155594,-0.201576935167323,330.083977400705));
#45039=CARTESIAN_POINT('Ctrl Pts',(170.164693744418,-0.338484202491844,
330.091496349901));
#45040=CARTESIAN_POINT('Ctrl Pts',(170.156935932896,-0.47494405665984,330.104735839044));
#45041=CARTESIAN_POINT('Ctrl Pts',(170.149183959373,-0.611301220462109,
330.117965365051));
#45042=CARTESIAN_POINT('Ctrl Pts',(170.14143198585,-0.747211253796988,330.136906824743));
#45043=CARTESIAN_POINT('Ctrl Pts',(170.133680012327,-0.882161083087291,
330.161511094775));
#45044=CARTESIAN_POINT('Ctrl Pts',(170.125931321769,-1.01705376104355,330.186104944883));
#45045=CARTESIAN_POINT('Ctrl Pts',(170.118182631211,-1.15098666001239,330.21635676551));
#45046=CARTESIAN_POINT('Ctrl Pts',(170.110433940654,-1.28345377321459,330.252165812234));
#45047=CARTESIAN_POINT('Ctrl Pts',(170.102686862276,-1.41589332552739,330.287967408586));
#45048=CARTESIAN_POINT('Ctrl Pts',(170.094939783898,-1.54686732158466,330.32932382928));
#45049=CARTESIAN_POINT('Ctrl Pts',(170.08719270552,-1.67588225171733,330.376083722549));
#45050=CARTESIAN_POINT('Ctrl Pts',(170.079445562214,-1.80489826311936,330.42284400771));
#45051=CARTESIAN_POINT('Ctrl Pts',(170.071698418909,-1.9319548083658,330.475007722583));
#45052=CARTESIAN_POINT('Ctrl Pts',(170.063951275603,-2.05657616232355,330.5323745064));
#45053=CARTESIAN_POINT('Ctrl Pts',(170.056202390575,-2.18122553380696,330.589754187488));
#45054=CARTESIAN_POINT('Ctrl Pts',(170.048453505547,-2.30343826958043,330.652339101798));
#45055=CARTESIAN_POINT('Ctrl Pts',(170.040704620519,-2.42276151141272,330.719882043528));
#45056=CARTESIAN_POINT('Ctrl Pts',(170.032947510744,-2.54221140416723,330.787496676033));
#45057=CARTESIAN_POINT('Ctrl Pts',(170.025190400969,-2.65876533578624,330.860079655447));
#45058=CARTESIAN_POINT('Ctrl Pts',(170.017433291194,-2.77199734957368,330.937339079316));
#45059=CARTESIAN_POINT('Ctrl Pts',(170.009672036268,-2.88528987092869,331.01463978815));
#45060=CARTESIAN_POINT('Ctrl Pts',(170.001910781342,-2.99525662413858,331.096621687301));
#45061=CARTESIAN_POINT('Ctrl Pts',(169.994149526416,-3.10150405393699,331.182951969661));
#45062=CARTESIAN_POINT('Ctrl Pts',(169.986375856011,-3.20792144499722,331.269420352338));
#45063=CARTESIAN_POINT('Ctrl Pts',(169.978602185607,-3.3106073304452,331.360250759255));
#45064=CARTESIAN_POINT('Ctrl Pts',(169.970828515202,-3.40920375800942,331.45507224349));
#45065=CARTESIAN_POINT('Ctrl Pts',(169.963416711025,-3.50321049815017,331.545479764822));
#45066=CARTESIAN_POINT('Ctrl Pts',(169.956004906848,-3.59349974155205,331.639514948513));
#45067=CARTESIAN_POINT('Ctrl Pts',(169.948593102671,-3.67979606917959,331.736829156825));
#45068=CARTESIAN_POINT('Ctrl Pts',(169.940888249857,-3.76950438942144,331.837990983791));
#45069=CARTESIAN_POINT('Ctrl Pts',(169.933183397044,-3.85519379095433,331.943030722558));
#45070=CARTESIAN_POINT('Ctrl Pts',(169.925478544231,-3.93650558769228,332.051592494147));
#45071=CARTESIAN_POINT('Ctrl Pts',(169.917785908505,-4.01768845356278,332.159982126344));
#45072=CARTESIAN_POINT('Ctrl Pts',(169.91009327278,-4.0945072985029,332.271882355992));
#45073=CARTESIAN_POINT('Ctrl Pts',(169.902400637055,-4.16664149157643,332.386901887955));
#45074=CARTESIAN_POINT('Ctrl Pts',(169.894715036249,-4.23870971788721,332.501816234487));
#45075=CARTESIAN_POINT('Ctrl Pts',(169.887029435444,-4.30610160079548,332.619843875871));
#45076=CARTESIAN_POINT('Ctrl Pts',(169.879343834638,-4.3685377832728,332.740561862184));
#45077=CARTESIAN_POINT('Ctrl Pts',(169.871663523159,-4.43093099638733,332.861196768867));
#45078=CARTESIAN_POINT('Ctrl Pts',(169.863983211681,-4.48837511010907,332.984517985316));
#45079=CARTESIAN_POINT('Ctrl Pts',(169.856302900202,-4.5406352564568,333.110075522588));
#45080=CARTESIAN_POINT('Ctrl Pts',(169.848626136853,-4.59287125979836,333.235575055116));
#45081=CARTESIAN_POINT('Ctrl Pts',(169.840949373505,-4.63992790790951,333.363308485592));
#45082=CARTESIAN_POINT('Ctrl Pts',(169.833272610157,-4.68161750597623,333.492803732012));
#45083=CARTESIAN_POINT('Ctrl Pts',(169.8255959283,-4.72330666149022,333.622297603785));
#45084=CARTESIAN_POINT('Ctrl Pts',(169.817919246444,-4.75962874628732,333.753552878788));
#45085=CARTESIAN_POINT('Ctrl Pts',(169.810242564587,-4.79044526993776,333.886080264009));
#45086=CARTESIAN_POINT('Ctrl Pts',(169.802566164899,-4.8212606608792,334.018602777981));
#45087=CARTESIAN_POINT('Ctrl Pts',(169.794889765211,-4.84657080862806,334.152396919398));
#45088=CARTESIAN_POINT('Ctrl Pts',(169.787213365523,-4.86628809491317,334.286961964685));
#45089=CARTESIAN_POINT('Ctrl Pts',(169.77953231574,-4.8860173252431,334.421608524786));
#45090=CARTESIAN_POINT('Ctrl Pts',(169.771851265956,-4.90014687278142,334.557026526107));
#45091=CARTESIAN_POINT('Ctrl Pts',(169.764170216173,-4.90864086521297,334.692708739367));
#45092=CARTESIAN_POINT('Ctrl Pts',(169.758292226945,-4.91514096577472,334.79654071682));
#45093=CARTESIAN_POINT('Ctrl Pts',(169.752414237718,-4.91834182617851,334.900527260846));
#45094=CARTESIAN_POINT('Ctrl Pts',(169.74653624849,-4.91824799493239,335.004441040815));
#45095=CARTESIAN_POINT('',(173.246536248458,-4.9182485732376,334.996253755704));
#45096=CARTESIAN_POINT('Ctrl Pts',(173.246536248458,-4.9182485732376,334.996253755704));
#45097=CARTESIAN_POINT('Ctrl Pts',(173.238884065945,-4.91835115497214,335.130927959976));
#45098=CARTESIAN_POINT('Ctrl Pts',(173.231231883431,-4.91291799432863,335.265810654158));
#45099=CARTESIAN_POINT('Ctrl Pts',(173.223579700918,-4.90192431480923,335.400401141834));
#45100=CARTESIAN_POINT('Ctrl Pts',(173.215935198301,-4.89094166878634,335.534856551561));
#45101=CARTESIAN_POINT('Ctrl Pts',(173.208290695685,-4.87440963568348,335.669019938917));
#45102=CARTESIAN_POINT('Ctrl Pts',(173.200646193069,-4.85235547248282,335.802389824939));
#45103=CARTESIAN_POINT('Ctrl Pts',(173.192669746678,-4.82934366134187,335.941550971119));
#45104=CARTESIAN_POINT('Ctrl Pts',(173.184693300287,-4.80031934116843,336.079847708487));
#45105=CARTESIAN_POINT('Ctrl Pts',(173.176716853896,-4.76537387231715,336.216714806163));
#45106=CARTESIAN_POINT('Ctrl Pts',(173.169081214905,-4.73192150876764,336.347734021528));
#45107=CARTESIAN_POINT('Ctrl Pts',(173.161445575915,-4.69304363311525,336.477442806396));
#45108=CARTESIAN_POINT('Ctrl Pts',(173.153809936924,-4.64887264541713,336.605355471287));
#45109=CARTESIAN_POINT('Ctrl Pts',(173.146175547409,-4.60470888574302,336.733247204888));
#45110=CARTESIAN_POINT('Ctrl Pts',(173.138541157894,-4.55525386766006,336.85934302168));
#45111=CARTESIAN_POINT('Ctrl Pts',(173.13090676838,-4.50068956887602,336.983173332594));
#45112=CARTESIAN_POINT('Ctrl Pts',(173.123271862838,-4.44612158196254,337.107012013489));
#45113=CARTESIAN_POINT('Ctrl Pts',(173.115636957297,-4.38644379067124,337.228584515003));
#45114=CARTESIAN_POINT('Ctrl Pts',(173.108002051756,-4.3218856996806,337.347442664134));
#45115=CARTESIAN_POINT('Ctrl Pts',(173.100364864461,-4.2573083149754,337.466336334997));
#45116=CARTESIAN_POINT('Ctrl Pts',(173.092727677166,-4.18784792324968,337.582513686413));
#45117=CARTESIAN_POINT('Ctrl Pts',(173.08509048987,-4.11377892183343,337.695553012793));
#45118=CARTESIAN_POINT('Ctrl Pts',(173.077445162384,-4.03963097304869,337.808712823548));
#45119=CARTESIAN_POINT('Ctrl Pts',(173.069799834897,-3.96086483198049,337.918727596373));
#45120=CARTESIAN_POINT('Ctrl Pts',(173.062154507411,-3.87779712334483,338.025206196721));
#45121=CARTESIAN_POINT('Ctrl Pts',(173.054504380427,-3.79467726740023,338.131751641003));
#45122=CARTESIAN_POINT('Ctrl Pts',(173.046854253443,-3.70725072930545,338.234756187929));
#45123=CARTESIAN_POINT('Ctrl Pts',(173.039204126459,-3.61587208542439,338.333864443007));
#45124=CARTESIAN_POINT('Ctrl Pts',(173.03154326898,-3.52436526876287,338.43311171285));
#45125=CARTESIAN_POINT('Ctrl Pts',(173.023882411502,-3.42889556893902,338.528451502177));
#45126=CARTESIAN_POINT('Ctrl Pts',(173.016221554023,-3.32985196175119,338.619567512193));
#45127=CARTESIAN_POINT('Ctrl Pts',(173.013884862577,-3.29964198194271,338.647359440425));
#45128=CARTESIAN_POINT('Ctrl Pts',(173.01154817113,-3.26909971494764,338.674758707052));
#45129=CARTESIAN_POINT('Ctrl Pts',(173.009211479684,-3.23823673494268,338.701757138302));
#45130=CARTESIAN_POINT('Ctrl Pts',(173.001436400905,-3.13554362959582,338.791591390992));
#45131=CARTESIAN_POINT('Ctrl Pts',(172.993661322127,-3.02894718200958,338.877291036297));
#45132=CARTESIAN_POINT('Ctrl Pts',(172.985886243349,-2.91881450009625,338.958497818179));
#45133=CARTESIAN_POINT('Ctrl Pts',(172.9781207323,-2.80881734345941,339.039604669947));
#45134=CARTESIAN_POINT('Ctrl Pts',(172.970355221251,-2.69529292244631,339.116229429175));
#45135=CARTESIAN_POINT('Ctrl Pts',(172.962589710202,-2.5786435038994,339.188052141783));
#45136=CARTESIAN_POINT('Ctrl Pts',(172.954831898679,-2.46210974359035,339.259803641964));
#45137=CARTESIAN_POINT('Ctrl Pts',(172.947074087157,-2.34245748252479,339.326762367052));
#45138=CARTESIAN_POINT('Ctrl Pts',(172.939316275635,-2.22011994459096,339.388650190449));
#45139=CARTESIAN_POINT('Ctrl Pts',(172.931564302112,-2.09787446953426,339.450491441297));
#45140=CARTESIAN_POINT('Ctrl Pts',(172.923812328589,-1.97294808720568,339.507269210311));
#45141=CARTESIAN_POINT('Ctrl Pts',(172.916060355066,-1.84580042180711,339.558750252575));
#45142=CARTESIAN_POINT('Ctrl Pts',(172.908311664508,-1.71870660352015,339.610209492588));
#45143=CARTESIAN_POINT('Ctrl Pts',(172.900562973951,-1.58939373472774,339.656376320962));
#45144=CARTESIAN_POINT('Ctrl Pts',(172.892814283393,-1.45834311253914,339.697064873792));
#45145=CARTESIAN_POINT('Ctrl Pts',(172.885067205015,-1.32731975652699,339.737744961029));
#45146=CARTESIAN_POINT('Ctrl Pts',(172.877320126637,-1.19455973933672,339.772948924038));
#45147=CARTESIAN_POINT('Ctrl Pts',(172.86957304826,-1.0605609019548,339.802540331506));
#45148=CARTESIAN_POINT('Ctrl Pts',(172.861825904954,-0.926560941533609,
339.83213198698));
#45149=CARTESIAN_POINT('Ctrl Pts',(172.854078761648,-0.791322521890436,
339.856110908803));
#45150=CARTESIAN_POINT('Ctrl Pts',(172.846331618342,-0.655354706495,339.87439157959));
#45151=CARTESIAN_POINT('Ctrl Pts',(172.838582733314,-0.519356322648134,
339.892676360259));
#45152=CARTESIAN_POINT('Ctrl Pts',(172.830833848286,-0.382628604052833,
339.905260288596));
#45153=CARTESIAN_POINT('Ctrl Pts',(172.823084963258,-0.245686385583616,
339.912109654969));
#45154=CARTESIAN_POINT('Ctrl Pts',(172.815327853483,-0.108598815228768,
339.91896629133));
#45155=CARTESIAN_POINT('Ctrl Pts',(172.807570743708,0.0287033187940506,
339.920076187369));
#45156=CARTESIAN_POINT('Ctrl Pts',(172.799813633934,0.165703968071794,339.915457787172));
#45157=CARTESIAN_POINT('Ctrl Pts',(172.792052379007,0.302777826116149,339.910836919049));
#45158=CARTESIAN_POINT('Ctrl Pts',(172.784291124081,0.439549488840512,339.90048168483));
#45159=CARTESIAN_POINT('Ctrl Pts',(172.776529869155,0.575508369748936,339.884462424756));
#45160=CARTESIAN_POINT('Ctrl Pts',(172.76875619875,0.711684740557825,339.868417539086));
#45161=CARTESIAN_POINT('Ctrl Pts',(172.760982528346,0.847045345256766,339.846690583788));
#45162=CARTESIAN_POINT('Ctrl Pts',(172.753208857941,0.981089243648321,339.819403174512));
#45163=CARTESIAN_POINT('Ctrl Pts',(172.745797053764,1.1088933663199,339.793386000703));
#45164=CARTESIAN_POINT('Ctrl Pts',(172.738385249587,1.23550032983211,339.76231446975));
#45165=CARTESIAN_POINT('Ctrl Pts',(172.73097344541,1.36049084386056,339.726335549479));
#45166=CARTESIAN_POINT('Ctrl Pts',(172.723198366632,1.49160751530998,339.688593195151));
#45167=CARTESIAN_POINT('Ctrl Pts',(172.715423287853,1.62135962966051,339.645330963759));
#45168=CARTESIAN_POINT('Ctrl Pts',(172.707648209075,1.74924725861172,339.596663691281));
#45169=CARTESIAN_POINT('Ctrl Pts',(172.699882698026,1.87697751369374,339.54805630698));
#45170=CARTESIAN_POINT('Ctrl Pts',(172.692117186977,2.00284748668668,339.494057253359));
#45171=CARTESIAN_POINT('Ctrl Pts',(172.684351675928,2.12637043170788,339.434831659675));
#45172=CARTESIAN_POINT('Ctrl Pts',(172.676593864405,2.24977090336935,339.37566478834));
#45173=CARTESIAN_POINT('Ctrl Pts',(172.668836052883,2.37082862790541,339.311281857578));
#45174=CARTESIAN_POINT('Ctrl Pts',(172.661078241361,2.48907528042128,339.241896664335));
#45175=CARTESIAN_POINT('Ctrl Pts',(172.653326267838,2.60723294858118,339.172563685651));
#45176=CARTESIAN_POINT('Ctrl Pts',(172.645574294315,2.72258341959847,339.098236134285));
#45177=CARTESIAN_POINT('Ctrl Pts',(172.637822320792,2.83468182381689,339.019174295825));
#45178=CARTESIAN_POINT('Ctrl Pts',(172.630073630234,2.94673275429471,338.940145940101));
#45179=CARTESIAN_POINT('Ctrl Pts',(172.622324939677,3.05553403847513,338.85638750985));
#45180=CARTESIAN_POINT('Ctrl Pts',(172.614576249119,3.16066892195133,338.768203156454));
#45181=CARTESIAN_POINT('Ctrl Pts',(172.606829170741,3.26578193123692,338.68003715055));
#45182=CARTESIAN_POINT('Ctrl Pts',(172.599082092363,3.36722975784459,338.587447304171));
#45183=CARTESIAN_POINT('Ctrl Pts',(172.591335013986,3.46462826344901,338.490778431612));
#45184=CARTESIAN_POINT('Ctrl Pts',(172.58358787068,3.56202758534641,338.394108748876));
#45185=CARTESIAN_POINT('Ctrl Pts',(172.575840727374,3.65537724112323,338.293360247122));
#45186=CARTESIAN_POINT('Ctrl Pts',(172.568093584068,3.74432983393046,338.188914730318));
#45187=CARTESIAN_POINT('Ctrl Pts',(172.56034469904,3.8333024251691,338.084445731944));
#45188=CARTESIAN_POINT('Ctrl Pts',(172.552595814012,3.91787573294078,337.976278362108));
#45189=CARTESIAN_POINT('Ctrl Pts',(172.544846928984,3.9977428034048,337.864827314224));
#45190=CARTESIAN_POINT('Ctrl Pts',(172.537089819209,4.07769464560279,337.753257971046));
#45191=CARTESIAN_POINT('Ctrl Pts',(172.529332709434,4.15293004397512,337.638398305767));
#45192=CARTESIAN_POINT('Ctrl Pts',(172.52157559966,4.22318524513987,337.520692255658));
#45193=CARTESIAN_POINT('Ctrl Pts',(172.513814344734,4.29347798843775,337.402923307199));
#45194=CARTESIAN_POINT('Ctrl Pts',(172.506053089807,4.35878504572007,337.2823052867));
#45195=CARTESIAN_POINT('Ctrl Pts',(172.498291834881,4.41888925994629,337.159305622378));
#45196=CARTESIAN_POINT('Ctrl Pts',(172.490518164477,4.47908962132733,337.036109198678));
#45197=CARTESIAN_POINT('Ctrl Pts',(172.482744494072,4.53407035128552,336.910523876191));
#45198=CARTESIAN_POINT('Ctrl Pts',(172.474970823667,4.58366263153101,336.783036719422));
#45199=CARTESIAN_POINT('Ctrl Pts',(172.46755901949,4.63094637919994,336.661484120472));
#45200=CARTESIAN_POINT('Ctrl Pts',(172.460147215313,4.67333195860183,336.538203035529));
#45201=CARTESIAN_POINT('Ctrl Pts',(172.452735411136,4.71071605606521,336.413625587498));
#45202=CARTESIAN_POINT('Ctrl Pts',(172.444960332358,4.74993245950672,336.282942227642));
#45203=CARTESIAN_POINT('Ctrl Pts',(172.437185253579,4.78376864041988,336.150419230752));
#45204=CARTESIAN_POINT('Ctrl Pts',(172.429410174801,4.81205062693849,336.016539141539));
#45205=CARTESIAN_POINT('Ctrl Pts',(172.421644663752,4.84029781067216,335.882823800299));
#45206=CARTESIAN_POINT('Ctrl Pts',(172.413879152703,4.86300431926685,335.747755068312));
#45207=CARTESIAN_POINT('Ctrl Pts',(172.406113641654,4.88004560731185,335.611831621491));
#45208=CARTESIAN_POINT('Ctrl Pts',(172.398355830131,4.89706999887007,335.476042943164));
#45209=CARTESIAN_POINT('Ctrl Pts',(172.390598018609,4.90844029987912,335.339401621821));
#45210=CARTESIAN_POINT('Ctrl Pts',(172.382840207087,4.91408285928114,335.202417179654));
#45211=CARTESIAN_POINT('Ctrl Pts',(172.375088233564,4.9197211724783,335.065535822624));
#45212=CARTESIAN_POINT('Ctrl Pts',(172.367336260041,4.91964030750197,334.928312247693));
#45213=CARTESIAN_POINT('Ctrl Pts',(172.359584286518,4.91381839955879,334.791261410713));
#45214=CARTESIAN_POINT('Ctrl Pts',(172.35183559596,4.90799895719709,334.654268614844));
#45215=CARTESIAN_POINT('Ctrl Pts',(172.344086905403,4.89644332417758,334.517448801137));
#45216=CARTESIAN_POINT('Ctrl Pts',(172.336338214845,4.87918173816371,334.381317021028));
#45217=CARTESIAN_POINT('Ctrl Pts',(172.328591136467,4.86192374356699,334.245213564273));
#45218=CARTESIAN_POINT('Ctrl Pts',(172.32084405809,4.83896220648185,334.109798243904));
#45219=CARTESIAN_POINT('Ctrl Pts',(172.313096979712,4.81037920931537,333.975580688836));
#45220=CARTESIAN_POINT('Ctrl Pts',(172.305349836406,4.78179597259581,333.841362008894));
#45221=CARTESIAN_POINT('Ctrl Pts',(172.2976026931,4.74759126323896,333.708341496577));
#45222=CARTESIAN_POINT('Ctrl Pts',(172.289855549794,4.70789815197728,333.577017901339));
#45223=CARTESIAN_POINT('Ctrl Pts',(172.282106664766,4.66819611686151,333.445664781769));
#45224=CARTESIAN_POINT('Ctrl Pts',(172.274357779738,4.62300333756766,333.316009712511));
#45225=CARTESIAN_POINT('Ctrl Pts',(172.26660889471,4.57250242829785,333.188535231999));
#45226=CARTESIAN_POINT('Ctrl Pts',(172.258851784935,4.52194791684115,333.060925448756));
#45227=CARTESIAN_POINT('Ctrl Pts',(172.251094675161,4.46607416494939,332.935501241658));
#45228=CARTESIAN_POINT('Ctrl Pts',(172.243337565386,4.40511175685733,332.812724646484));
#45229=CARTESIAN_POINT('Ctrl Pts',(172.23557631046,4.34411677240365,332.689882443424));
#45230=CARTESIAN_POINT('Ctrl Pts',(172.227815055533,4.27802790170672,332.569691013737));
#45231=CARTESIAN_POINT('Ctrl Pts',(172.220053800607,4.20712069899228,332.452585921643));
#45232=CARTESIAN_POINT('Ctrl Pts',(172.212280130203,4.13610006786209,332.335293499566));
#45233=CARTESIAN_POINT('Ctrl Pts',(172.204506459798,4.06024591871126,332.2210976067));
#45234=CARTESIAN_POINT('Ctrl Pts',(172.196732789393,3.97987647721037,332.110403784497));
#45235=CARTESIAN_POINT('Ctrl Pts',(172.189320985216,3.9032482525467,332.004862786349));
#45236=CARTESIAN_POINT('Ctrl Pts',(172.181909181039,3.82251582723015,331.902505379444));
#45237=CARTESIAN_POINT('Ctrl Pts',(172.174497376862,3.73798667367353,331.803652288949));
#45238=CARTESIAN_POINT('Ctrl Pts',(172.166722298084,3.64931449450228,331.699954114022));
#45239=CARTESIAN_POINT('Ctrl Pts',(172.158947219305,3.55618377817555,331.599784749845));
#45240=CARTESIAN_POINT('Ctrl Pts',(172.151172140527,3.45890616067516,331.5035516257));
#45241=CARTESIAN_POINT('Ctrl Pts',(172.143406629478,3.36174824947598,331.407436922542));
#45242=CARTESIAN_POINT('Ctrl Pts',(172.135641118429,3.26045386588272,331.315249093922));
#45243=CARTESIAN_POINT('Ctrl Pts',(172.12787560738,3.15537495844174,331.227362734884));
#45244=CARTESIAN_POINT('Ctrl Pts',(172.120117795857,3.05040023704328,331.139563515428));
#45245=CARTESIAN_POINT('Ctrl Pts',(172.112359984335,2.94164875711457,331.056057527278));
#45246=CARTESIAN_POINT('Ctrl Pts',(172.104602172813,2.82950912992339,330.977182436876));
#45247=CARTESIAN_POINT('Ctrl Pts',(172.09685019929,2.71745389135814,330.898366702481));
#45248=CARTESIAN_POINT('Ctrl Pts',(172.089098225767,2.60201589898342,330.824175153282));
#45249=CARTESIAN_POINT('Ctrl Pts',(172.081346252244,2.48361635786692,330.754904848012));
#45250=CARTESIAN_POINT('Ctrl Pts',(172.073597561686,2.36526695902625,330.685663878756));
#45251=CARTESIAN_POINT('Ctrl Pts',(172.065848871129,2.24395884266799,330.621340205175));
#45252=CARTESIAN_POINT('Ctrl Pts',(172.058100180571,2.12014148986842,330.562187123657));
#45253=CARTESIAN_POINT('Ctrl Pts',(172.050353102193,1.99634989830326,330.503046349431));
#45254=CARTESIAN_POINT('Ctrl Pts',(172.042606023816,1.87005046119664,330.449074195848));
#45255=CARTESIAN_POINT('Ctrl Pts',(172.034858945438,1.74171615587461,330.400477427508));
#45256=CARTESIAN_POINT('Ctrl Pts',(172.027111802132,1.61338077498778,330.35188025188));
#45257=CARTESIAN_POINT('Ctrl Pts',(172.019364658826,1.48301085741342,330.308658689773));
#45258=CARTESIAN_POINT('Ctrl Pts',(172.01161751552,1.35109782441841,330.270970741119));
#45259=CARTESIAN_POINT('Ctrl Pts',(172.003868630492,1.2191551345729,330.233274319414));
#45260=CARTESIAN_POINT('Ctrl Pts',(171.996119745464,1.0856690147272,330.201114094086));
#45261=CARTESIAN_POINT('Ctrl Pts',(171.988370860436,0.951144064768316,330.174597630191));
#45262=CARTESIAN_POINT('Ctrl Pts',(171.980613750661,0.816476328637388,330.148053021448));
#45263=CARTESIAN_POINT('Ctrl Pts',(171.972856640887,0.680767943897373,330.127164216128));
#45264=CARTESIAN_POINT('Ctrl Pts',(171.965099531112,0.544532228650927,330.1119873451));
#45265=CARTESIAN_POINT('Ctrl Pts',(171.957338276186,0.408223713394111,330.096802364038));
#45266=CARTESIAN_POINT('Ctrl Pts',(171.94957702126,0.271387695886138,330.087335426165));
#45267=CARTESIAN_POINT('Ctrl Pts',(171.941815766333,0.134539569573238,330.083590520846));
#45268=CARTESIAN_POINT('Ctrl Pts',(171.934042095929,-0.00252746914292362,
330.079839624898));
#45269=CARTESIAN_POINT('Ctrl Pts',(171.926268425524,-0.139606264332587,
330.081829047007));
#45270=CARTESIAN_POINT('Ctrl Pts',(171.918494755119,-0.276183577365626,
330.089510646168));
#45271=CARTESIAN_POINT('Ctrl Pts',(171.911082950942,-0.406403183618759,
330.09683466504));
#45272=CARTESIAN_POINT('Ctrl Pts',(171.903671146765,-0.536166658549343,
330.109332817696));
#45273=CARTESIAN_POINT('Ctrl Pts',(171.896259342588,-0.66503790655522,330.126920106817));
#45274=CARTESIAN_POINT('Ctrl Pts',(171.88848426381,-0.800225518313382,330.145369401367));
#45275=CARTESIAN_POINT('Ctrl Pts',(171.880709185031,-0.934858448114493,
330.16947761691));
#45276=CARTESIAN_POINT('Ctrl Pts',(171.872934106253,-1.06842543586947,330.199203175463));
#45277=CARTESIAN_POINT('Ctrl Pts',(171.865168595204,-1.20182806094268,330.228892154824));
#45278=CARTESIAN_POINT('Ctrl Pts',(171.857403084155,-1.33416697600323,330.264184639206));
#45279=CARTESIAN_POINT('Ctrl Pts',(171.849637573106,-1.46493671653396,330.30498738244));
#45280=CARTESIAN_POINT('Ctrl Pts',(171.841879761584,-1.59557679848631,330.345749669635));
#45281=CARTESIAN_POINT('Ctrl Pts',(171.834121950061,-1.72465043139156,330.392011227458));
#45282=CARTESIAN_POINT('Ctrl Pts',(171.826364138539,-1.85166336448089,330.443627995089));
#45283=CARTESIAN_POINT('Ctrl Pts',(171.818612165016,-1.9785807163094,330.495205919465));
#45284=CARTESIAN_POINT('Ctrl Pts',(171.810860191493,-2.10344009434181,330.552130885633));
#45285=CARTESIAN_POINT('Ctrl Pts',(171.80310821797,-2.22576375732302,330.614209448789));
#45286=CARTESIAN_POINT('Ctrl Pts',(171.795359527413,-2.34803561616103,330.676261721638));
#45287=CARTESIAN_POINT('Ctrl Pts',(171.787610836855,-2.4677735479811,330.743463074013));
#45288=CARTESIAN_POINT('Ctrl Pts',(171.779862146297,-2.5845213104435,330.815572600897));
#45289=CARTESIAN_POINT('Ctrl Pts',(171.77211506792,-2.70124478255856,330.887667124792));
#45290=CARTESIAN_POINT('Ctrl Pts',(171.764367989542,-2.81497899043046,330.96466758671));
#45291=CARTESIAN_POINT('Ctrl Pts',(171.756620911164,-2.92529410612515,331.046288142116));
#45292=CARTESIAN_POINT('Ctrl Pts',(171.748873767858,-3.03561014636689,331.127909381582));
#45293=CARTESIAN_POINT('Ctrl Pts',(171.741126624552,-3.14250672305798,331.214150559282));
#45294=CARTESIAN_POINT('Ctrl Pts',(171.733379481247,-3.24558503444035,331.304683931418));
#45295=CARTESIAN_POINT('Ctrl Pts',(171.725630596219,-3.34868652001539,331.395237657379));
#45296=CARTESIAN_POINT('Ctrl Pts',(171.71788171119,-3.44796773848256,331.49008524008));
#45297=CARTESIAN_POINT('Ctrl Pts',(171.710132826162,-3.54306516813837,331.588860560337));
#45298=CARTESIAN_POINT('Ctrl Pts',(171.702375716388,-3.63826353518874,331.687740721739));
#45299=CARTESIAN_POINT('Ctrl Pts',(171.694618606613,-3.72926897115358,331.790556666521));
#45300=CARTESIAN_POINT('Ctrl Pts',(171.686861496838,-3.81575648850863,331.896907110171));
#45301=CARTESIAN_POINT('Ctrl Pts',(171.679100241912,-3.90229022202734,332.003314384098));
#45302=CARTESIAN_POINT('Ctrl Pts',(171.671338986986,-3.98430099277517,332.113259607193));
#45303=CARTESIAN_POINT('Ctrl Pts',(171.66357773206,-4.06150653704379,332.226311532985));
#45304=CARTESIAN_POINT('Ctrl Pts',(171.655804061655,-4.13883558502221,332.339544305015));
#45305=CARTESIAN_POINT('Ctrl Pts',(171.64803039125,-4.21134383918479,332.455893378795));
#45306=CARTESIAN_POINT('Ctrl Pts',(171.640256720846,-4.2787940394573,332.574901109149));
#45307=CARTESIAN_POINT('Ctrl Pts',(171.632844916669,-4.34310441667927,332.688369001024));
#45308=CARTESIAN_POINT('Ctrl Pts',(171.625433112491,-4.40281691558553,332.804253343021));
#45309=CARTESIAN_POINT('Ctrl Pts',(171.618021308314,-4.45776701588196,332.922141416117));
#45310=CARTESIAN_POINT('Ctrl Pts',(171.609572694798,-4.52040387851417,333.056520407251));
#45311=CARTESIAN_POINT('Ctrl Pts',(171.601124081281,-4.57702589321632,333.193873629242));
#45312=CARTESIAN_POINT('Ctrl Pts',(171.592675467765,-4.62736511960204,333.333664165785));
#45313=CARTESIAN_POINT('Ctrl Pts',(171.584255967307,-4.6775308821615,333.472972998434));
#45314=CARTESIAN_POINT('Ctrl Pts',(171.575836466848,-4.72145694007028,333.614702130559));
#45315=CARTESIAN_POINT('Ctrl Pts',(171.56741696639,-4.75892347987298,333.758295375215));
#45316=CARTESIAN_POINT('Ctrl Pts',(171.559015379067,-4.79631030672791,333.901583114188));
#45317=CARTESIAN_POINT('Ctrl Pts',(171.550613791744,-4.82726493948641,334.04672678951));
#45318=CARTESIAN_POINT('Ctrl Pts',(171.542212204421,-4.85161628364152,334.193152741342));
#45319=CARTESIAN_POINT('Ctrl Pts',(171.533839254757,-4.87588462378235,334.339079585538));
#45320=CARTESIAN_POINT('Ctrl Pts',(171.525466305092,-4.89359451160953,334.486279713807));
#45321=CARTESIAN_POINT('Ctrl Pts',(171.517093355428,-4.90462539132199,334.634168299215));
#45322=CARTESIAN_POINT('Ctrl Pts',(171.510240986461,-4.91365299340367,334.755199380713));
#45323=CARTESIAN_POINT('Ctrl Pts',(171.503388617494,-4.91820808107563,334.876691189428));
#45324=CARTESIAN_POINT('Ctrl Pts',(171.496536248527,-4.91824971188751,334.998316545704));
#45325=CARTESIAN_POINT('',(174.996536248523,-4.91824863027879,335.003670594061));
#45326=CARTESIAN_POINT('Ctrl Pts',(174.99653624849,-4.91824863027836,335.003670594644));
#45327=CARTESIAN_POINT('Ctrl Pts',(174.98331673886,-4.91807501968798,335.236292317054));
#45328=CARTESIAN_POINT('Ctrl Pts',(174.970097229231,-4.90139623116265,335.468309461225));
#45329=CARTESIAN_POINT('Ctrl Pts',(174.956877719601,-4.86847588454197,335.697943854571));
#45330=CARTESIAN_POINT('Ctrl Pts',(174.949102640823,-4.84911372243734,335.833003743216));
#45331=CARTESIAN_POINT('Ctrl Pts',(174.941327562044,-4.82409651574911,335.967470732522));
#45332=CARTESIAN_POINT('Ctrl Pts',(174.933552483266,-4.79346929543573,336.100833854955));
#45333=CARTESIAN_POINT('Ctrl Pts',(174.925786972217,-4.76287976386681,336.234032865575));
#45334=CARTESIAN_POINT('Ctrl Pts',(174.918021461168,-4.72669404126795,336.366130334791));
#45335=CARTESIAN_POINT('Ctrl Pts',(174.910255950119,-4.68500878645265,336.496621439564));
#45336=CARTESIAN_POINT('Ctrl Pts',(174.902498138597,-4.6433648626888,336.626983162026));
#45337=CARTESIAN_POINT('Ctrl Pts',(174.894740327074,-4.59623237626986,336.7557413197));
#45338=CARTESIAN_POINT('Ctrl Pts',(174.886982515552,-4.54375872374385,336.882402646328));
#45339=CARTESIAN_POINT('Ctrl Pts',(174.879230542029,-4.49132455930545,337.008968656291));
#45340=CARTESIAN_POINT('Ctrl Pts',(174.871478568506,-4.43355737817314,337.133440616346));
#45341=CARTESIAN_POINT('Ctrl Pts',(174.863726594983,-4.37065384821781,337.255342102999));
#45342=CARTESIAN_POINT('Ctrl Pts',(174.855977904425,-4.30777695794471,337.377191964299));
#45343=CARTESIAN_POINT('Ctrl Pts',(174.848229213868,-4.23976822412976,337.496473170708));
#45344=CARTESIAN_POINT('Ctrl Pts',(174.84048052331,-4.16687162853289,337.612731117782));
#45345=CARTESIAN_POINT('Ctrl Pts',(174.832733444932,-4.09399019968162,337.728964876419));
#45346=CARTESIAN_POINT('Ctrl Pts',(174.824986366554,-4.01622313936925,337.842176295924));
#45347=CARTESIAN_POINT('Ctrl Pts',(174.817239288177,-3.93385918940115,337.951937489254));
#45348=CARTESIAN_POINT('Ctrl Pts',(174.809492144871,-3.85149454914383,338.061699602489));
#45349=CARTESIAN_POINT('Ctrl Pts',(174.801745001565,-3.76453317699013,338.168011119234));
#45350=CARTESIAN_POINT('Ctrl Pts',(174.793997858259,-3.67330550344933,338.270475460973));
#45351=CARTESIAN_POINT('Ctrl Pts',(174.786248973231,-3.58205731999085,338.372962838872));
#45352=CARTESIAN_POINT('Ctrl Pts',(174.778500088203,-3.48654118640158,338.471601028783));
#45353=CARTESIAN_POINT('Ctrl Pts',(174.770751203175,-3.38712566936063,338.566028990692));
#45354=CARTESIAN_POINT('Ctrl Pts',(174.7629940934,-3.28760463166257,338.660557179417));
#45355=CARTESIAN_POINT('Ctrl Pts',(174.755236983625,-3.18417622663505,338.75086594372));
#45356=CARTESIAN_POINT('Ctrl Pts',(174.747479873851,-3.07724392515281,338.836633014456));
#45357=CARTESIAN_POINT('Ctrl Pts',(174.739718618925,-2.97025448246778,338.922445916372));
#45358=CARTESIAN_POINT('Ctrl Pts',(174.731957363998,-2.85975772718503,339.003712057366));
#45359=CARTESIAN_POINT('Ctrl Pts',(174.724196109072,-2.74618680282642,339.080152093548));
#45360=CARTESIAN_POINT('Ctrl Pts',(174.716422438668,-2.63243420200145,339.156714408876));
#45361=CARTESIAN_POINT('Ctrl Pts',(174.708648768263,-2.51559793843602,339.228434987562));
#45362=CARTESIAN_POINT('Ctrl Pts',(174.700875097858,-2.39613724972105,339.295079666665));
#45363=CARTESIAN_POINT('Ctrl Pts',(174.693463293681,-2.28223748480732,339.358622019922));
#45364=CARTESIAN_POINT('Ctrl Pts',(174.686051489504,-2.16595238685683,339.417550274945));
#45365=CARTESIAN_POINT('Ctrl Pts',(174.678639685327,-2.04769577692535,339.471702703408));
#45366=CARTESIAN_POINT('Ctrl Pts',(174.670864606549,-1.92364305827191,339.528509303701));
#45367=CARTESIAN_POINT('Ctrl Pts',(174.66308952777,-1.79702865221146,339.580239604505));
#45368=CARTESIAN_POINT('Ctrl Pts',(174.655314448992,-1.66830661107918,339.626654959464));
#45369=CARTESIAN_POINT('Ctrl Pts',(174.647548937943,-1.53974297061342,339.673013197373));
#45370=CARTESIAN_POINT('Ctrl Pts',(174.639783426894,-1.40907721973958,339.714069371594));
#45371=CARTESIAN_POINT('Ctrl Pts',(174.632017915845,-1.27678618255062,339.749631575875));
#45372=CARTESIAN_POINT('Ctrl Pts',(174.624260104323,-1.14462631231009,339.785158520126));
#45373=CARTESIAN_POINT('Ctrl Pts',(174.616502292801,-1.0108447377249,339.815202234028));
#45374=CARTESIAN_POINT('Ctrl Pts',(174.608744481278,-0.875936021643368,
339.839619731806));
#45375=CARTESIAN_POINT('Ctrl Pts',(174.600992507755,-0.741128828649,339.864018854643));
#45376=CARTESIAN_POINT('Ctrl Pts',(174.593240534232,-0.60519656555478,339.882800119406));
#45377=CARTESIAN_POINT('Ctrl Pts',(174.585488560709,-0.46864629531195,339.895871088212));
#45378=CARTESIAN_POINT('Ctrl Pts',(174.577739870152,-0.332153854189639,
339.908936521455));
#45379=CARTESIAN_POINT('Ctrl Pts',(174.569991179594,-0.195044314760044,
339.91629643143));
#45380=CARTESIAN_POINT('Ctrl Pts',(174.562242489037,-0.0578319961281068,
339.917909975053));
#45381=CARTESIAN_POINT('Ctrl Pts',(174.554495410659,0.0793517743349073,
339.919523182965));
#45382=CARTESIAN_POINT('Ctrl Pts',(174.546748332281,0.216637890863955,339.915392398025));
#45383=CARTESIAN_POINT('Ctrl Pts',(174.539001253903,0.353510279357964,339.905528875146));
#45384=CARTESIAN_POINT('Ctrl Pts',(174.531254110597,0.490383814974363,339.895665269601));
#45385=CARTESIAN_POINT('Ctrl Pts',(174.523506967292,0.626843225776368,339.880068858382));
#45386=CARTESIAN_POINT('Ctrl Pts',(174.515759823986,0.762376205521692,339.858802896162));
#45387=CARTESIAN_POINT('Ctrl Pts',(174.508010938958,0.897939655958299,339.837532152903));
#45388=CARTESIAN_POINT('Ctrl Pts',(174.50026205393,1.03257587480725,339.810589382839));
#45389=CARTESIAN_POINT('Ctrl Pts',(174.492513168902,1.16578180324149,339.778089142087));
#45390=CARTESIAN_POINT('Ctrl Pts',(174.484756059127,1.29912911782448,339.745554405244));
#45391=CARTESIAN_POINT('Ctrl Pts',(174.476998949352,1.4310427290607,339.707450507188));
#45392=CARTESIAN_POINT('Ctrl Pts',(174.469241839577,1.56103329270892,339.66394233686));
#45393=CARTESIAN_POINT('Ctrl Pts',(174.461480584651,1.69109331915798,339.620410917157));
#45394=CARTESIAN_POINT('Ctrl Pts',(174.453719329725,1.81922788544291,339.571469610237));
#45395=CARTESIAN_POINT('Ctrl Pts',(174.445958074799,1.94496768651358,339.517331486721));
#45396=CARTESIAN_POINT('Ctrl Pts',(174.438184404394,2.07090863028747,339.463106759851));
#45397=CARTESIAN_POINT('Ctrl Pts',(174.43041073399,2.19444680127458,339.403668773679));
#45398=CARTESIAN_POINT('Ctrl Pts',(174.422637063585,2.31513676705072,339.33927699189));
#45399=CARTESIAN_POINT('Ctrl Pts',(174.415225259408,2.43020858588388,339.277882663036));
#45400=CARTESIAN_POINT('Ctrl Pts',(174.407813455231,2.54269115165218,339.211985503431));
#45401=CARTESIAN_POINT('Ctrl Pts',(174.400401651054,2.65222452123518,339.141845983551));
#45402=CARTESIAN_POINT('Ctrl Pts',(174.392626572275,2.76712644754428,339.068268716868));
#45403=CARTESIAN_POINT('Ctrl Pts',(174.384851493497,2.87914588136086,338.989790195661));
#45404=CARTESIAN_POINT('Ctrl Pts',(174.377076414718,2.98783642609918,338.906663096989));
#45405=CARTESIAN_POINT('Ctrl Pts',(174.369310903669,3.09639322020262,338.823638291504));
#45406=CARTESIAN_POINT('Ctrl Pts',(174.36154539262,3.20162896839791,338.735976525637));
#45407=CARTESIAN_POINT('Ctrl Pts',(174.353779881571,3.30312425574478,338.643974919454));
#45408=CARTESIAN_POINT('Ctrl Pts',(174.346022070049,3.40451891021875,338.552064533132));
#45409=CARTESIAN_POINT('Ctrl Pts',(174.338264258527,3.50218019658619,338.455823130458));
#45410=CARTESIAN_POINT('Ctrl Pts',(174.330506447005,3.59572023872465,338.355589222078));
#45411=CARTESIAN_POINT('Ctrl Pts',(174.322754473482,3.689189889015,338.255430742892));
#45412=CARTESIAN_POINT('Ctrl Pts',(174.315002499959,3.77854420258656,338.151286022901));
#45413=CARTESIAN_POINT('Ctrl Pts',(174.307250526436,3.8634310455938,338.043531438714));
#45414=CARTESIAN_POINT('Ctrl Pts',(174.299501835878,3.94828193897268,337.935822488658));
#45415=CARTESIAN_POINT('Ctrl Pts',(174.29175314532,4.02866888341605,337.824507021447));
#45416=CARTESIAN_POINT('Ctrl Pts',(174.284004454763,4.10427920552521,337.709995436453));
#45417=CARTESIAN_POINT('Ctrl Pts',(174.276257376385,4.17987379627534,337.59550767655));
#45418=CARTESIAN_POINT('Ctrl Pts',(174.268510298007,4.25069352622226,337.477825447534));
#45419=CARTESIAN_POINT('Ctrl Pts',(174.260763219629,4.31646858255452,337.357388817807));
#45420=CARTESIAN_POINT('Ctrl Pts',(174.253016076323,4.38224419014507,337.236951178704));
#45421=CARTESIAN_POINT('Ctrl Pts',(174.245268933018,4.44297485244015,337.113759435894));
#45422=CARTESIAN_POINT('Ctrl Pts',(174.237521789712,4.4984365233414,336.98827862936));
#45423=CARTESIAN_POINT('Ctrl Pts',(174.229772904684,4.55391066320374,336.862769612076));
#45424=CARTESIAN_POINT('Ctrl Pts',(174.222024019656,4.60411329650204,336.73497086445));
#45425=CARTESIAN_POINT('Ctrl Pts',(174.214275134627,4.64886852192176,336.605367412272));
#45426=CARTESIAN_POINT('Ctrl Pts',(174.206518024853,4.69367125100018,336.47562639765));
#45427=CARTESIAN_POINT('Ctrl Pts',(174.198760915078,4.7330148944555,336.344077222069));
#45428=CARTESIAN_POINT('Ctrl Pts',(174.191003805303,4.76677329866749,336.211220616408));
#45429=CARTESIAN_POINT('Ctrl Pts',(174.183242550377,4.8005497422913,336.078293016424));
#45430=CARTESIAN_POINT('Ctrl Pts',(174.175481295451,4.82873491936202,335.944056976578));
#45431=CARTESIAN_POINT('Ctrl Pts',(174.167720040525,4.85125403761879,335.809022450237));
#45432=CARTESIAN_POINT('Ctrl Pts',(174.15994637012,4.87380917912581,335.673771912662));
#45433=CARTESIAN_POINT('Ctrl Pts',(174.152172699715,4.89068010144037,335.537720724239));
#45434=CARTESIAN_POINT('Ctrl Pts',(174.144399029311,4.90184394406614,335.401383869285));
#45435=CARTESIAN_POINT('Ctrl Pts',(174.136987225134,4.91248810713189,335.271393527729));
#45436=CARTESIAN_POINT('Ctrl Pts',(174.129575420956,4.91794455035138,335.141143804223));
#45437=CARTESIAN_POINT('Ctrl Pts',(174.122163616779,4.91823752302836,335.011078338136));
#45438=CARTESIAN_POINT('Ctrl Pts',(174.114388538001,4.91854485516896,334.874637976112));
#45439=CARTESIAN_POINT('Ctrl Pts',(174.106613459222,4.91317073573236,334.737969213465));
#45440=CARTESIAN_POINT('Ctrl Pts',(174.098838380444,4.9020860754402,334.60158417266));
#45441=CARTESIAN_POINT('Ctrl Pts',(174.091072869395,4.89101505552821,334.46536696233));
#45442=CARTESIAN_POINT('Ctrl Pts',(174.083307358346,4.87424750820317,334.329433165025));
#45443=CARTESIAN_POINT('Ctrl Pts',(174.075541847297,4.85180631857765,334.194296264431));
#45444=CARTESIAN_POINT('Ctrl Pts',(174.067784035775,4.82938737945698,334.059293352468));
#45445=CARTESIAN_POINT('Ctrl Pts',(174.060026224253,4.80130605658553,333.925086147932));
#45446=CARTESIAN_POINT('Ctrl Pts',(174.05226841273,4.76763710875924,333.792184011663));
#45447=CARTESIAN_POINT('Ctrl Pts',(174.044516439207,4.7339934978839,333.659381888467));
#45448=CARTESIAN_POINT('Ctrl Pts',(174.036764465684,4.69477072723567,333.527883256083));
#45449=CARTESIAN_POINT('Ctrl Pts',(174.029012492161,4.6500947401073,333.398187910357));
#45450=CARTESIAN_POINT('Ctrl Pts',(174.021263801604,4.605437673286,333.268547490687));
#45451=CARTESIAN_POINT('Ctrl Pts',(174.013515111046,4.55533211033673,333.140709207536));
#45452=CARTESIAN_POINT('Ctrl Pts',(174.005766420489,4.49995395932998,333.015158085285));
#45453=CARTESIAN_POINT('Ctrl Pts',(173.998019342111,4.44458733021006,332.889633084993));
#45454=CARTESIAN_POINT('Ctrl Pts',(173.990272263733,4.38395045269997,332.766394656483));
#45455=CARTESIAN_POINT('Ctrl Pts',(173.982525185355,4.3182673785125,332.645907837366));
#45456=CARTESIAN_POINT('Ctrl Pts',(173.974778042049,4.25258375383766,332.525420008453));
#45457=CARTESIAN_POINT('Ctrl Pts',(173.967030898744,4.18185403522065,332.407684178123));
#45458=CARTESIAN_POINT('Ctrl Pts',(173.959283755438,4.10634804050459,332.293140411336));
#45459=CARTESIAN_POINT('Ctrl Pts',(173.95153487041,4.03082507043788,332.178570892678));
#45460=CARTESIAN_POINT('Ctrl Pts',(173.943785985382,3.95052390259725,332.067195191881));
#45461=CARTESIAN_POINT('Ctrl Pts',(173.936037100353,3.86575721522074,331.959423703396));
#45462=CARTESIAN_POINT('Ctrl Pts',(173.928279990579,3.78090055560641,331.85153782514));
#45463=CARTESIAN_POINT('Ctrl Pts',(173.920522880804,3.69156915039299,331.747264108802));
#45464=CARTESIAN_POINT('Ctrl Pts',(173.912765771029,3.59811580589651,331.646979613862));
#45465=CARTESIAN_POINT('Ctrl Pts',(173.905004516103,3.5046125229208,331.546641530095));
#45466=CARTESIAN_POINT('Ctrl Pts',(173.897243261177,3.40698318979185,331.450297189768));
#45467=CARTESIAN_POINT('Ctrl Pts',(173.889482006251,3.30561616279193,331.358285452319));
#45468=CARTESIAN_POINT('Ctrl Pts',(173.881708335846,3.20408698158427,331.266126526077));
#45469=CARTESIAN_POINT('Ctrl Pts',(173.873934665441,3.09880845883244,331.178314302906));
#45470=CARTESIAN_POINT('Ctrl Pts',(173.866160995037,2.99020128470804,331.09514669425));
#45471=CARTESIAN_POINT('Ctrl Pts',(173.85874919086,2.88664980066902,331.015850557785));
#45472=CARTESIAN_POINT('Ctrl Pts',(173.851337386683,2.78007282393473,330.940776519158));
#45473=CARTESIAN_POINT('Ctrl Pts',(173.843925582506,2.67085654300497,330.87014426533));
#45474=CARTESIAN_POINT('Ctrl Pts',(173.836150503727,2.55628724680781,330.796050114339));
#45475=CARTESIAN_POINT('Ctrl Pts',(173.828375424949,2.4384513242031,330.726610016504));
#45476=CARTESIAN_POINT('Ctrl Pts',(173.82060034617,2.31776368802125,330.662125572473));
#45477=CARTESIAN_POINT('Ctrl Pts',(173.812834835121,2.19722456565895,330.597720480656));
#45478=CARTESIAN_POINT('Ctrl Pts',(173.805069324072,2.07384105350507,330.53825909132));
#45479=CARTESIAN_POINT('Ctrl Pts',(173.797303813023,1.94805733539498,330.484000035373));
#45480=CARTESIAN_POINT('Ctrl Pts',(173.789546001501,1.82239833220769,330.429794777438));
#45481=CARTESIAN_POINT('Ctrl Pts',(173.781788189979,1.69434421561682,330.380781741747));
#45482=CARTESIAN_POINT('Ctrl Pts',(173.774030378457,1.5643637742931,330.337173706412));
#45483=CARTESIAN_POINT('Ctrl Pts',(173.766278404934,1.43448114737362,330.293598487506));
#45484=CARTESIAN_POINT('Ctrl Pts',(173.758526431411,1.3026754502025,330.255420296752));
#45485=CARTESIAN_POINT('Ctrl Pts',(173.750774457888,1.16943512690991,330.222803693959));
#45486=CARTESIAN_POINT('Ctrl Pts',(173.74302576733,1.03625123097314,330.190200904317));
#45487=CARTESIAN_POINT('Ctrl Pts',(173.735277076772,0.901634296192913,330.163155110784));
#45488=CARTESIAN_POINT('Ctrl Pts',(173.727528386215,0.766087383869004,330.141780863035));
#45489=CARTESIAN_POINT('Ctrl Pts',(173.719781307837,0.630568673212303,330.120411062376));
#45490=CARTESIAN_POINT('Ctrl Pts',(173.712034229459,0.494120755737382,330.104710521219));
#45491=CARTESIAN_POINT('Ctrl Pts',(173.704287151081,0.357255938731466,330.094742488234));
#45492=CARTESIAN_POINT('Ctrl Pts',(173.696540007775,0.220389974666582,330.084774371707));
#45493=CARTESIAN_POINT('Ctrl Pts',(173.688792864469,0.0831074939433382,
330.080538887571));
#45494=CARTESIAN_POINT('Ctrl Pts',(173.681045721164,-0.0540754295057921,
330.082047284649));
#45495=CARTESIAN_POINT('Ctrl Pts',(173.673296836136,-0.191289194588415,
330.083556020847));
#45496=CARTESIAN_POINT('Ctrl Pts',(173.665547951107,-0.32840296708379,330.090811203597));
#45497=CARTESIAN_POINT('Ctrl Pts',(173.657799066079,-0.464902429405222,
330.103771983084));
#45498=CARTESIAN_POINT('Ctrl Pts',(173.650041956305,-0.601546773666418,
330.116746519276));
#45499=CARTESIAN_POINT('Ctrl Pts',(173.64228484653,-0.737575115513532,330.135438712587));
#45500=CARTESIAN_POINT('Ctrl Pts',(173.634527736755,-0.87247945384309,330.159755929179));
#45501=CARTESIAN_POINT('Ctrl Pts',(173.626766481829,-1.00745588073751,330.184086140113));
#45502=CARTESIAN_POINT('Ctrl Pts',(173.619005226903,-1.1413067260601,330.214047278384));
#45503=CARTESIAN_POINT('Ctrl Pts',(173.611243971977,-1.27353687381356,330.249496143193));
#45504=CARTESIAN_POINT('Ctrl Pts',(173.603470301572,-1.40597854670977,330.285001714633));
#45505=CARTESIAN_POINT('Ctrl Pts',(173.595696631167,-1.53679396810694,330.326012437812));
#45506=CARTESIAN_POINT('Ctrl Pts',(173.587922960763,-1.66550495832667,330.372335762365));
#45507=CARTESIAN_POINT('Ctrl Pts',(173.580511156585,-1.78822442098549,330.416502725015));
#45508=CARTESIAN_POINT('Ctrl Pts',(173.573099352408,-1.90903069919843,330.465498708422));
#45509=CARTESIAN_POINT('Ctrl Pts',(173.565687548231,-2.02753006475578,330.519117843659));
#45510=CARTESIAN_POINT('Ctrl Pts',(173.557912469453,-2.15183743721038,330.575365012438));
#45511=CARTESIAN_POINT('Ctrl Pts',(173.550137390674,-2.273998876064,330.636877732265));
#45512=CARTESIAN_POINT('Ctrl Pts',(173.542362311896,-2.39353622575786,330.703470307506));
#45513=CARTESIAN_POINT('Ctrl Pts',(173.534596800847,-2.51292647713295,330.769980936344));
#45514=CARTESIAN_POINT('Ctrl Pts',(173.526831289798,-2.62969872614955,330.841558794322));
#45515=CARTESIAN_POINT('Ctrl Pts',(173.519065778749,-2.74339511119906,330.917970317802));
#45516=CARTESIAN_POINT('Ctrl Pts',(173.511307967227,-2.8569787659517,330.994306079033));
#45517=CARTESIAN_POINT('Ctrl Pts',(173.503550155705,-2.96749230354208,331.075465751609));
#45518=CARTESIAN_POINT('Ctrl Pts',(173.495792344182,-3.07450310586851,331.161170267581));
#45519=CARTESIAN_POINT('Ctrl Pts',(173.488040370659,-3.18143337917254,331.246810288186));
#45520=CARTESIAN_POINT('Ctrl Pts',(173.480288397136,-3.28486586002153,331.336988101208));
#45521=CARTESIAN_POINT('Ctrl Pts',(173.472536423613,-3.38439784141672,331.43138201631));
#45522=CARTESIAN_POINT('Ctrl Pts',(173.464787733056,-3.4838876709588,331.525735955534));
#45523=CARTESIAN_POINT('Ctrl Pts',(173.457039042498,-3.57948000346481,331.624302177149));
#45524=CARTESIAN_POINT('Ctrl Pts',(173.449290351941,-3.67080627633533,331.726719635577));
#45525=CARTESIAN_POINT('Ctrl Pts',(173.441543273563,-3.76211354801196,331.829115785198));
#45526=CARTESIAN_POINT('Ctrl Pts',(173.433796195185,-3.84915626555285,331.935361286274));
#45527=CARTESIAN_POINT('Ctrl Pts',(173.426049116807,-3.93160400293221,332.045059556162));
#45528=CARTESIAN_POINT('Ctrl Pts',(173.418301973501,-4.01405243130296,332.154758745428));
#45529=CARTESIAN_POINT('Ctrl Pts',(173.410554830196,-4.09190556785868,332.267910448764));
#45530=CARTESIAN_POINT('Ctrl Pts',(173.40280768689,-4.16487467600814,332.384086775972));
#45531=CARTESIAN_POINT('Ctrl Pts',(173.395058801862,-4.2378601891622,332.500289222084));
#45532=CARTESIAN_POINT('Ctrl Pts',(173.387309916834,-4.30595928108932,332.619517314258));
#45533=CARTESIAN_POINT('Ctrl Pts',(173.379561031806,-4.36892797651213,332.741316445681));
#45534=CARTESIAN_POINT('Ctrl Pts',(173.371803922031,-4.43196350755898,332.863244855962));
#45535=CARTESIAN_POINT('Ctrl Pts',(173.364046812256,-4.48985758450184,332.987749409016));
#45536=CARTESIAN_POINT('Ctrl Pts',(173.356289702482,-4.54241319656434,333.114352786395));
#45537=CARTESIAN_POINT('Ctrl Pts',(173.348528447556,-4.59499689266553,333.24102381657));
#45538=CARTESIAN_POINT('Ctrl Pts',(173.340767192629,-4.64223630506473,333.369795539072));
#45539=CARTESIAN_POINT('Ctrl Pts',(173.333005937703,-4.68398391869246,333.500174106128));
#45540=CARTESIAN_POINT('Ctrl Pts',(173.325232267299,-4.72579831489646,333.6307612364));
#45541=CARTESIAN_POINT('Ctrl Pts',(173.317458596894,-4.76210325355548,333.762959970584));
#45542=CARTESIAN_POINT('Ctrl Pts',(173.309684926489,-4.79280188391725,333.896263997136));
#45543=CARTESIAN_POINT('Ctrl Pts',(173.302273122312,-4.82207148565075,334.023362689183));
#45544=CARTESIAN_POINT('Ctrl Pts',(173.294861318135,-4.84624492692439,334.151465803835));
#45545=CARTESIAN_POINT('Ctrl Pts',(173.287449513958,-4.86528225838518,334.28013083915));
#45546=CARTESIAN_POINT('Ctrl Pts',(173.273811758802,-4.90031103937786,334.516875119869));
#45547=CARTESIAN_POINT('Ctrl Pts',(173.260174003646,-4.91806575156673,334.756236763849));
#45548=CARTESIAN_POINT('Ctrl Pts',(173.24653624849,-4.91824857323717,334.996253755141));
#45549=CARTESIAN_POINT('',(176.746536248452,-4.91824967172903,335.001796952215));
#45550=CARTESIAN_POINT('Ctrl Pts',(176.746536248452,-4.91824967172903,335.001796952215));
#45551=CARTESIAN_POINT('Ctrl Pts',(176.738150524747,-4.91819529342756,335.150630104864));
#45552=CARTESIAN_POINT('Ctrl Pts',(176.729764801042,-4.91138089118401,335.299258443303));
#45553=CARTESIAN_POINT('Ctrl Pts',(176.721379077337,-4.89788709035797,335.447085129035));
#45554=CARTESIAN_POINT('Ctrl Pts',(176.712958450813,-4.88433712601955,335.595527094777));
#45555=CARTESIAN_POINT('Ctrl Pts',(176.704537824288,-4.86405212912126,335.743160447532));
#45556=CARTESIAN_POINT('Ctrl Pts',(176.696117197763,-4.8371644110477,335.889395032027));
#45557=CARTESIAN_POINT('Ctrl Pts',(176.687678931725,-4.81022036862904,336.035935948474));
#45558=CARTESIAN_POINT('Ctrl Pts',(176.679240665686,-4.77664603317014,336.181071971229));
#45559=CARTESIAN_POINT('Ctrl Pts',(176.670802399648,-4.73662377549646,336.324227424539));
#45560=CARTESIAN_POINT('Ctrl Pts',(176.66233646536,-4.69647028875198,336.467852270588));
#45561=CARTESIAN_POINT('Ctrl Pts',(176.653870531072,-4.64982665521896,336.60948328444));
#45562=CARTESIAN_POINT('Ctrl Pts',(176.645404596783,-4.59692468450908,336.748561267857));
#45563=CARTESIAN_POINT('Ctrl Pts',(176.639038372937,-4.55714339446076,336.853145303639));
#45564=CARTESIAN_POINT('Ctrl Pts',(176.632672149091,-4.51382416144281,336.95628609718));
#45565=CARTESIAN_POINT('Ctrl Pts',(176.626305925245,-4.46708249308073,337.05775534564));
#45566=CARTESIAN_POINT('Ctrl Pts',(176.618530846466,-4.40999682306017,337.181679891722));
#45567=CARTESIAN_POINT('Ctrl Pts',(176.610755767688,-4.34766021946007,337.303422980626));
#45568=CARTESIAN_POINT('Ctrl Pts',(176.602980688909,-4.28026160395896,337.422507722212));
#45569=CARTESIAN_POINT('Ctrl Pts',(176.59521517786,-4.21294592674504,337.541445922442));
#45570=CARTESIAN_POINT('Ctrl Pts',(176.587449666811,-4.14058082249508,337.657731947315));
#45571=CARTESIAN_POINT('Ctrl Pts',(176.579684155762,-4.06340294269931,337.770909523561));
#45572=CARTESIAN_POINT('Ctrl Pts',(176.571926344239,-3.98630158499605,337.883974883911));
#45573=CARTESIAN_POINT('Ctrl Pts',(176.564168532717,-3.90439716685733,337.993937608203));
#45574=CARTESIAN_POINT('Ctrl Pts',(176.556410721194,-3.81797167250749,338.10036697351));
#45575=CARTESIAN_POINT('Ctrl Pts',(176.548658747671,-3.73161121608271,338.206716247345));
#45576=CARTESIAN_POINT('Ctrl Pts',(176.540906774148,-3.64073670087276,338.309537152526));
#45577=CARTESIAN_POINT('Ctrl Pts',(176.533154800625,-3.54567253044435,338.408429164491));
#45578=CARTESIAN_POINT('Ctrl Pts',(176.525406110067,-3.45064861974863,338.50727929563));
#45579=CARTESIAN_POINT('Ctrl Pts',(176.517657419509,-3.35143885315349,338.602203561708));
#45580=CARTESIAN_POINT('Ctrl Pts',(176.509908728951,-3.24840675790063,338.692835847655));
#45581=CARTESIAN_POINT('Ctrl Pts',(176.502161650573,-3.1453960993357,338.783449276798));
#45582=CARTESIAN_POINT('Ctrl Pts',(176.494414572195,-3.03856498725729,338.869772244013));
#45583=CARTESIAN_POINT('Ctrl Pts',(176.486667493817,-2.92831222752099,338.951477010012));
#45584=CARTESIAN_POINT('Ctrl Pts',(176.478920350511,-2.81805854376046,339.033182460775));
#45585=CARTESIAN_POINT('Ctrl Pts',(176.471173207205,-2.70438346918492,339.110269400398));
#45586=CARTESIAN_POINT('Ctrl Pts',(176.463426063899,-2.58771683484811,339.18245198958));
#45587=CARTESIAN_POINT('Ctrl Pts',(176.455677178871,-2.47102397137492,339.254650806941));
#45588=CARTESIAN_POINT('Ctrl Pts',(176.447928293843,-2.35133854214129,339.32194287419));
#45589=CARTESIAN_POINT('Ctrl Pts',(176.440179408815,-2.2291167918094,339.384087292809));
#45590=CARTESIAN_POINT('Ctrl Pts',(176.43242229904,-2.1067653140489,339.446297672157));
#45591=CARTESIAN_POINT('Ctrl Pts',(176.424665189265,-1.98187248648536,339.50334931105));
#45592=CARTESIAN_POINT('Ctrl Pts',(176.41690807949,-1.85491694762461,339.555048427834));
#45593=CARTESIAN_POINT('Ctrl Pts',(176.409146824564,-1.72789356778323,339.606775170973));
#45594=CARTESIAN_POINT('Ctrl Pts',(176.401385569637,-1.59880564799407,339.653143560695));
#45595=CARTESIAN_POINT('Ctrl Pts',(176.393624314711,-1.46814802133065,339.694009421589));
#45596=CARTESIAN_POINT('Ctrl Pts',(176.385850644306,-1.33728138504572,339.734940654542));
#45597=CARTESIAN_POINT('Ctrl Pts',(176.378076973901,-1.2048404019347,339.770351668144));
#45598=CARTESIAN_POINT('Ctrl Pts',(176.370303303496,-1.07133202628335,339.800149034349));
#45599=CARTESIAN_POINT('Ctrl Pts',(176.362891499321,-0.944038497675528,
339.828559325979));
#45600=CARTESIAN_POINT('Ctrl Pts',(176.355479695146,-0.815774997577205,
339.851866787858));
#45601=CARTESIAN_POINT('Ctrl Pts',(176.348067890971,-0.686984287717369,
339.870034460959));
#45602=CARTESIAN_POINT('Ctrl Pts',(176.340292812193,-0.551881161484992,
339.889092585842));
#45603=CARTESIAN_POINT('Ctrl Pts',(176.332517733414,-0.415770887673747,
339.902554577005));
#45604=CARTESIAN_POINT('Ctrl Pts',(176.324742654636,-0.279156729737768,
339.910321230097));
#45605=CARTESIAN_POINT('Ctrl Pts',(176.316977143587,-0.142710684220461,
339.918078325828));
#45606=CARTESIAN_POINT('Ctrl Pts',(176.309211632538,-0.00576237483657899,
339.920154006373));
#45607=CARTESIAN_POINT('Ctrl Pts',(176.301446121489,0.131176442785312,339.916500361371));
#45608=CARTESIAN_POINT('Ctrl Pts',(176.293688309967,0.267979485170984,339.912850338968));
#45609=CARTESIAN_POINT('Ctrl Pts',(176.285930498445,0.404772666305083,339.903482306176));
#45610=CARTESIAN_POINT('Ctrl Pts',(176.278172686923,0.541041184245535,339.888400300656));
#45611=CARTESIAN_POINT('Ctrl Pts',(176.2704207134,0.677207155804843,339.873329644822));
#45612=CARTESIAN_POINT('Ctrl Pts',(176.262668739877,0.812848863114032,339.852553617917));
#45613=CARTESIAN_POINT('Ctrl Pts',(176.254916766354,0.94745394314014,339.826128270998));
#45614=CARTESIAN_POINT('Ctrl Pts',(176.247168075796,1.08200201783484,339.799714115229));
#45615=CARTESIAN_POINT('Ctrl Pts',(176.239419385239,1.21551395565618,339.767655473082));
#45616=CARTESIAN_POINT('Ctrl Pts',(176.231670694681,1.3474851571824,339.730059916499));
#45617=CARTESIAN_POINT('Ctrl Pts',(176.223923616303,1.47942890099786,339.692472181986));
#45618=CARTESIAN_POINT('Ctrl Pts',(176.216176537926,1.60983217045877,339.649349931471));
#45619=CARTESIAN_POINT('Ctrl Pts',(176.208429459548,1.7382035458745,339.600851170774));
#45620=CARTESIAN_POINT('Ctrl Pts',(176.200682316242,1.86657599716592,339.55235200361));
#45621=CARTESIAN_POINT('Ctrl Pts',(176.192935172936,1.99291615479683,339.498476374529));
#45622=CARTESIAN_POINT('Ctrl Pts',(176.185188029631,2.11675104415547,339.439431053589));
#45623=CARTESIAN_POINT('Ctrl Pts',(176.177439144603,2.24061377422634,339.380372458006));
#45624=CARTESIAN_POINT('Ctrl Pts',(176.169690259575,2.36196976249369,339.316142025998));
#45625=CARTESIAN_POINT('Ctrl Pts',(176.161941374547,2.48036953208909,339.246993059423));
#45626=CARTESIAN_POINT('Ctrl Pts',(176.154184264772,2.59889497242325,339.17777069742));
#45627=CARTESIAN_POINT('Ctrl Pts',(176.146427154997,2.71445758805366,339.103619569682));
#45628=CARTESIAN_POINT('Ctrl Pts',(176.138670045223,2.82663540509307,339.024837307168));
#45629=CARTESIAN_POINT('Ctrl Pts',(176.130908790297,2.93887316637111,338.946012945932));
#45630=CARTESIAN_POINT('Ctrl Pts',(176.12314753537,3.04772221497418,338.862552756513));
#45631=CARTESIAN_POINT('Ctrl Pts',(176.115386280444,3.15279352815466,338.774794833011));
#45632=CARTESIAN_POINT('Ctrl Pts',(176.10761261004,3.25803292119363,338.686896525432));
#45633=CARTESIAN_POINT('Ctrl Pts',(176.099838939635,3.35948221341567,338.594687008579));
#45634=CARTESIAN_POINT('Ctrl Pts',(176.092065269231,3.45678849712969,338.498542031849));
#45635=CARTESIAN_POINT('Ctrl Pts',(176.084653465053,3.54956514993692,338.406872626906));
#45636=CARTESIAN_POINT('Ctrl Pts',(176.077241660875,3.63857563156937,338.311626118262));
#45637=CARTESIAN_POINT('Ctrl Pts',(176.069829856697,3.72354925861636,338.213154833051));
#45638=CARTESIAN_POINT('Ctrl Pts',(176.062054777919,3.81268769623886,338.109857176832));
#45639=CARTESIAN_POINT('Ctrl Pts',(176.05427969914,3.89766525097212,338.002684199664));
#45640=CARTESIAN_POINT('Ctrl Pts',(176.046504620362,3.97812615503005,337.892005421358));
#45641=CARTESIAN_POINT('Ctrl Pts',(176.038739109313,4.05848804682317,337.781462840335));
#45642=CARTESIAN_POINT('Ctrl Pts',(176.030973598264,4.1343441191766,337.667423355154));
#45643=CARTESIAN_POINT('Ctrl Pts',(176.023208087215,4.20537714291025,337.550291384997));
#45644=CARTESIAN_POINT('Ctrl Pts',(176.015450275693,4.27633973719405,337.433275551528));
#45645=CARTESIAN_POINT('Ctrl Pts',(176.00769246417,4.34248859806439,337.313173667076));
#45646=CARTESIAN_POINT('Ctrl Pts',(175.999934652648,4.4035485320052,337.190420824585));
#45647=CARTESIAN_POINT('Ctrl Pts',(175.992182679125,4.46456251640938,337.067760357501));
#45648=CARTESIAN_POINT('Ctrl Pts',(175.984430705602,4.52049502309245,336.942453251748));
#45649=CARTESIAN_POINT('Ctrl Pts',(175.976678732079,4.57111591754807,336.814960696775));
#45650=CARTESIAN_POINT('Ctrl Pts',(175.968930041521,4.62171537402483,336.687522134975));
#45651=CARTESIAN_POINT('Ctrl Pts',(175.961181350964,4.66700754837085,336.557900327318));
#45652=CARTESIAN_POINT('Ctrl Pts',(175.953432660406,4.70680983242573,336.426577815571));
#45653=CARTESIAN_POINT('Ctrl Pts',(175.945685582028,4.74660383528297,336.29528262657));
#45654=CARTESIAN_POINT('Ctrl Pts',(175.937938503651,4.78091010649549,336.16228781114));
#45655=CARTESIAN_POINT('Ctrl Pts',(175.930191425273,4.8095955811343,336.028092120597));
#45656=CARTESIAN_POINT('Ctrl Pts',(175.922444281967,4.83828129618499,335.893895305365));
#45657=CARTESIAN_POINT('Ctrl Pts',(175.914697138661,4.86134603899531,335.758497977184));
#45658=CARTESIAN_POINT('Ctrl Pts',(175.906949995355,4.87870773321556,335.622409765639));
#45659=CARTESIAN_POINT('Ctrl Pts',(175.899201110327,4.89607333071325,335.486290958575));
#45660=CARTESIAN_POINT('Ctrl Pts',(175.891452225299,4.90773327879709,335.349481346722));
#45661=CARTESIAN_POINT('Ctrl Pts',(175.883703340271,4.91365734668025,335.212495980939));
#45662=CARTESIAN_POINT('Ctrl Pts',(175.875946230496,4.91958770243027,335.075365217474));
#45663=CARTESIAN_POINT('Ctrl Pts',(175.868189120722,4.91976999946911,334.938058718559));
#45664=CARTESIAN_POINT('Ctrl Pts',(175.860432010947,4.91422616773608,334.801092396229));
#45665=CARTESIAN_POINT('Ctrl Pts',(175.852670756021,4.90867937355664,334.664052883476));
#45666=CARTESIAN_POINT('Ctrl Pts',(175.844909501095,4.89740038568387,334.527354298872));
#45667=CARTESIAN_POINT('Ctrl Pts',(175.837148246168,4.8804629921296,334.391506742064));
#45668=CARTESIAN_POINT('Ctrl Pts',(175.829374575764,4.86349850426553,334.255441873438));
#45669=CARTESIAN_POINT('Ctrl Pts',(175.821600905359,4.8408575875193,334.120231138731));
#45670=CARTESIAN_POINT('Ctrl Pts',(175.813827234954,4.81266523897367,333.986374645111));
#45671=CARTESIAN_POINT('Ctrl Pts',(175.806415430777,4.78578525103527,333.858749203471));
#45672=CARTESIAN_POINT('Ctrl Pts',(175.7990036266,4.75385910895547,333.732355039452));
#45673=CARTESIAN_POINT('Ctrl Pts',(175.791591822423,4.71703660981305,333.607610440939));
#45674=CARTESIAN_POINT('Ctrl Pts',(175.783816743645,4.67840933029932,333.476751738058));
#45675=CARTESIAN_POINT('Ctrl Pts',(175.776041664866,4.63427151824114,333.347294851836));
#45676=CARTESIAN_POINT('Ctrl Pts',(175.768266586088,4.58474138436665,333.219738923367));
#45677=CARTESIAN_POINT('Ctrl Pts',(175.760501075039,4.53527220047513,333.092339960588));
#45678=CARTESIAN_POINT('Ctrl Pts',(175.75273556399,4.48042403783168,332.966837662012));
#45679=CARTESIAN_POINT('Ctrl Pts',(175.744970052941,4.42036531024096,332.843717646847));
#45680=CARTESIAN_POINT('Ctrl Pts',(175.737212241418,4.36036613105347,332.720719705536));
#45681=CARTESIAN_POINT('Ctrl Pts',(175.729454429896,4.29516683839358,332.600099696084));
#45682=CARTESIAN_POINT('Ctrl Pts',(175.721696618374,4.22498438819908,332.482324488348));
#45683=CARTESIAN_POINT('Ctrl Pts',(175.713944644851,4.15485475252395,332.36463791019));
#45684=CARTESIAN_POINT('Ctrl Pts',(175.706192671328,4.07974962275891,332.249792207009));
#45685=CARTESIAN_POINT('Ctrl Pts',(175.698440697805,3.99993228396393,332.138230479895));
#45686=CARTESIAN_POINT('Ctrl Pts',(175.690692007247,3.92014874785933,332.026715999238));
#45687=CARTESIAN_POINT('Ctrl Pts',(175.682943316689,3.83565719884264,331.918483045743));
#45688=CARTESIAN_POINT('Ctrl Pts',(175.675194626132,3.74676459682838,331.813946309546));
#45689=CARTESIAN_POINT('Ctrl Pts',(175.667447547754,3.65789048966241,331.709431323091));
#45690=CARTESIAN_POINT('Ctrl Pts',(175.659700469376,3.56461740389315,331.608611321866));
#45691=CARTESIAN_POINT('Ctrl Pts',(175.651953390998,3.46729274107458,331.511868105964));
#45692=CARTESIAN_POINT('Ctrl Pts',(175.644206247692,3.36996726258167,331.415124079261));
#45693=CARTESIAN_POINT('Ctrl Pts',(175.636459104387,3.26859041652813,331.322457181591));
#45694=CARTESIAN_POINT('Ctrl Pts',(175.628711961081,3.16354634508102,331.234212222519));
#45695=CARTESIAN_POINT('Ctrl Pts',(175.620963076053,3.0584786574965,331.145947424106));
#45696=CARTESIAN_POINT('Ctrl Pts',(175.613214191025,2.94974240313968,331.062106793901));
#45697=CARTESIAN_POINT('Ctrl Pts',(175.605465305996,2.83775433965222,330.98299447719));
#45698=CARTESIAN_POINT('Ctrl Pts',(175.597708196222,2.72564741087706,330.903798189849));
#45699=CARTESIAN_POINT('Ctrl Pts',(175.589951086447,2.61028209802139,330.829340467172));
#45700=CARTESIAN_POINT('Ctrl Pts',(175.582193976672,2.49210411006948,330.75988205741));
#45701=CARTESIAN_POINT('Ctrl Pts',(175.574432721746,2.37386297157946,330.690386531295));
#45702=CARTESIAN_POINT('Ctrl Pts',(175.56667146682,2.25280650792318,330.625895824932));
#45703=CARTESIAN_POINT('Ctrl Pts',(175.558910211894,2.12940360370253,330.566623932595));
#45704=CARTESIAN_POINT('Ctrl Pts',(175.551136541489,2.005803295052,330.507257224547));
#45705=CARTESIAN_POINT('Ctrl Pts',(175.543362871084,1.87984940445537,330.453126167522));
#45706=CARTESIAN_POINT('Ctrl Pts',(175.53558920068,1.75203012579135,330.40439628549));
#45707=CARTESIAN_POINT('Ctrl Pts',(175.528177396503,1.63016086530532,330.357934791191));
#45708=CARTESIAN_POINT('Ctrl Pts',(175.520765592326,1.50659624888517,330.316383030537));
#45709=CARTESIAN_POINT('Ctrl Pts',(175.513353788149,1.3817690875308,330.279841395541));
#45710=CARTESIAN_POINT('Ctrl Pts',(175.505578709371,1.25082377515307,330.241508746162));
#45711=CARTESIAN_POINT('Ctrl Pts',(175.497803630592,1.11807521495644,330.208568624591));
#45712=CARTESIAN_POINT('Ctrl Pts',(175.490028551814,0.984007115942841,330.181191738793));
#45713=CARTESIAN_POINT('Ctrl Pts',(175.482263040765,0.850103996260252,330.153848541996));
#45714=CARTESIAN_POINT('Ctrl Pts',(175.474497529716,0.714884947920567,330.132055037017));
#45715=CARTESIAN_POINT('Ctrl Pts',(175.466732018667,0.578849476850443,330.115932397514));
#45716=CARTESIAN_POINT('Ctrl Pts',(175.458974207145,0.442948885345953,330.099825743656));
#45717=CARTESIAN_POINT('Ctrl Pts',(175.451216395622,0.306233867690224,330.08937881153));
#45718=CARTESIAN_POINT('Ctrl Pts',(175.4434585841,0.169214432013063,330.084661808329));
#45719=CARTESIAN_POINT('Ctrl Pts',(175.435706610577,0.0322981078065591,
330.079948354823));
#45720=CARTESIAN_POINT('Ctrl Pts',(175.427954637054,-0.104921789370491,
330.080956260904));
#45721=CARTESIAN_POINT('Ctrl Pts',(175.420202663531,-0.241930167705256,
330.087703911972));
#45722=CARTESIAN_POINT('Ctrl Pts',(175.412453972974,-0.378880522910594,
330.094448705406));
#45723=CARTESIAN_POINT('Ctrl Pts',(175.404705282416,-0.515619147850069,
330.106928389981));
#45724=CARTESIAN_POINT('Ctrl Pts',(175.396956591859,-0.651631207117099,
330.125109249182));
#45725=CARTESIAN_POINT('Ctrl Pts',(175.389209513481,-0.787614967939216,
330.143286325704));
#45726=CARTESIAN_POINT('Ctrl Pts',(175.381462435103,-0.922872076587738,
330.167162165707));
#45727=CARTESIAN_POINT('Ctrl Pts',(175.373715356725,-1.05689347030419,330.196651245753));
#45728=CARTESIAN_POINT('Ctrl Pts',(175.365968213419,-1.19091598724888,330.226140572945));
#45729=CARTESIAN_POINT('Ctrl Pts',(175.358221070114,-1.32370238686213,330.261243150017));
#45730=CARTESIAN_POINT('Ctrl Pts',(175.350473926808,-1.45475483005692,330.301822539864));
#45731=CARTESIAN_POINT('Ctrl Pts',(175.34272504178,-1.58583673662319,330.34241105282));
#45732=CARTESIAN_POINT('Ctrl Pts',(175.334976156752,-1.7151835377412,330.388478713116));
#45733=CARTESIAN_POINT('Ctrl Pts',(175.327227271723,-1.84231393967725,330.439839650827));
#45734=CARTESIAN_POINT('Ctrl Pts',(175.319470161949,-1.96957927913551,330.491255103567));
#45735=CARTESIAN_POINT('Ctrl Pts',(175.311713052174,-2.0946231570666,330.547974910234));
#45736=CARTESIAN_POINT('Ctrl Pts',(175.303955942399,-2.21698510599749,330.609765370474));
#45737=CARTESIAN_POINT('Ctrl Pts',(175.296194687473,-2.3394124412415,330.671588849561));
#45738=CARTESIAN_POINT('Ctrl Pts',(175.288433432547,-2.45915465077377,330.738488190786));
#45739=CARTESIAN_POINT('Ctrl Pts',(175.280672177621,-2.57577804188075,330.810184903666));
#45740=CARTESIAN_POINT('Ctrl Pts',(175.272898507216,-2.69258799240602,330.881996307921));
#45741=CARTESIAN_POINT('Ctrl Pts',(175.265124836812,-2.80626883052823,330.958620200636));
#45742=CARTESIAN_POINT('Ctrl Pts',(175.257351166407,-2.91641717388945,331.039735623681));
#45743=CARTESIAN_POINT('Ctrl Pts',(175.24993936223,-3.0214380853683,331.117075104269));
#45744=CARTESIAN_POINT('Ctrl Pts',(175.242527558053,-3.12324775145683,331.198497184425));
#45745=CARTESIAN_POINT('Ctrl Pts',(175.235115753875,-3.22152753150027,331.283692232028));
#45746=CARTESIAN_POINT('Ctrl Pts',(175.227453993813,-3.32312170152013,331.371760399735));
#45747=CARTESIAN_POINT('Ctrl Pts',(175.21979223375,-3.42128496967472,331.464156638968));
#45748=CARTESIAN_POINT('Ctrl Pts',(175.212130473687,-3.51561789539192,331.560579427273));
#45749=CARTESIAN_POINT('Ctrl Pts',(175.204478209541,-3.60983390571463,331.656882710026));
#45750=CARTESIAN_POINT('Ctrl Pts',(175.196825945396,-3.70022873512071,331.757202332378));
#45751=CARTESIAN_POINT('Ctrl Pts',(175.189173681251,-3.78643552622414,331.861196236104));
#45752=CARTESIAN_POINT('Ctrl Pts',(175.181147121554,-3.87685895410756,331.970276798476));
#45753=CARTESIAN_POINT('Ctrl Pts',(175.173120561857,-3.96267393582545,332.083399904661));
#45754=CARTESIAN_POINT('Ctrl Pts',(175.16509400216,-4.04349958118173,332.200126038643));
#45755=CARTESIAN_POINT('Ctrl Pts',(175.157455179504,-4.1204208020118,332.311213512045));
#45756=CARTESIAN_POINT('Ctrl Pts',(175.149816356847,-4.19282314218833,332.425563705027));
#45757=CARTESIAN_POINT('Ctrl Pts',(175.142177534191,-4.26041931293051,332.542763678335));
#45758=CARTESIAN_POINT('Ctrl Pts',(175.134541627137,-4.32798968342031,332.659918918504));
#45759=CARTESIAN_POINT('Ctrl Pts',(175.126905720083,-4.39075733081347,332.779921427516));
#45760=CARTESIAN_POINT('Ctrl Pts',(175.119269813029,-4.44847898427495,332.902330390895));
#45761=CARTESIAN_POINT('Ctrl Pts',(175.111635055533,-4.50619194795037,333.024720926047));
#45762=CARTESIAN_POINT('Ctrl Pts',(175.104000298038,-4.55886025722331,333.149516830151));
#45763=CARTESIAN_POINT('Ctrl Pts',(175.096365540542,-4.60628745153904,333.27625437599));
#45764=CARTESIAN_POINT('Ctrl Pts',(175.08873016777,-4.65371846795447,333.403002135453));
#45765=CARTESIAN_POINT('Ctrl Pts',(175.081094794998,-4.69590738979103,333.531691469616));
#45766=CARTESIAN_POINT('Ctrl Pts',(175.073459422227,-4.73270678457583,333.661840983392));
#45767=CARTESIAN_POINT('Ctrl Pts',(175.065818297401,-4.76953390192671,333.792088544391));
#45768=CARTESIAN_POINT('Ctrl Pts',(175.058177172575,-4.80096327696741,333.923798092651));
#45769=CARTESIAN_POINT('Ctrl Pts',(175.050536047748,-4.8268980031814,334.056475368958));
#45770=CARTESIAN_POINT('Ctrl Pts',(175.042891561909,-4.85284413700427,334.189211004488));
#45771=CARTESIAN_POINT('Ctrl Pts',(175.035247076069,-4.87329074815301,334.322914817622));
#45772=CARTESIAN_POINT('Ctrl Pts',(175.02760259023,-4.88819266699765,334.457086090793));
#45773=CARTESIAN_POINT('Ctrl Pts',(175.019949266185,-4.90311181476041,334.591412486664));
#45774=CARTESIAN_POINT('Ctrl Pts',(175.01229594214,-4.91247344731158,334.726207020056));
#45775=CARTESIAN_POINT('Ctrl Pts',(175.004642618094,-4.91628447297953,334.860967474164));
#45776=CARTESIAN_POINT('Ctrl Pts',(175.001940494904,-4.91763001392046,334.908546715035));
#45777=CARTESIAN_POINT('Ctrl Pts',(174.999238371714,-4.91828411700569,334.956121738744));
#45778=CARTESIAN_POINT('Ctrl Pts',(174.996536248523,-4.91824863027879,335.003670594061));
#45779=CARTESIAN_POINT('',(178.49653624852,-4.91824801907883,334.995585781249));
#45780=CARTESIAN_POINT('Ctrl Pts',(178.49653624849,-4.9182480190793,334.995585781775));
#45781=CARTESIAN_POINT('Ctrl Pts',(178.488851432236,-4.91836997075314,335.131462294372));
#45782=CARTESIAN_POINT('Ctrl Pts',(178.481166615983,-4.9128568937543,335.267459173279));
#45783=CARTESIAN_POINT('Ctrl Pts',(178.473481799729,-4.90170571785073,335.403068378925));
#45784=CARTESIAN_POINT('Ctrl Pts',(178.465800244587,-4.8905592740358,335.538620037746));
#45785=CARTESIAN_POINT('Ctrl Pts',(178.458118689445,-4.87377952071571,335.67378395427));
#45786=CARTESIAN_POINT('Ctrl Pts',(178.450437134304,-4.8514154582341,335.808053905446));
#45787=CARTESIAN_POINT('Ctrl Pts',(178.442757111446,-4.82905585684227,335.942297073014));
#45788=CARTESIAN_POINT('Ctrl Pts',(178.435077088589,-4.80111422662373,336.075646237142));
#45789=CARTESIAN_POINT('Ctrl Pts',(178.427397065732,-4.76769116346065,336.207602597032));
#45790=CARTESIAN_POINT('Ctrl Pts',(178.419716841635,-4.7342672245123,336.339562414578));
#45791=CARTESIAN_POINT('Ctrl Pts',(178.412036617538,-4.69536166472711,336.470128969166));
#45792=CARTESIAN_POINT('Ctrl Pts',(178.404356393441,-4.65112558195678,336.598816400769));
#45793=CARTESIAN_POINT('Ctrl Pts',(178.396674234723,-4.60687835627982,336.727536248262));
#45794=CARTESIAN_POINT('Ctrl Pts',(178.388992076006,-4.55729806644526,336.854375654774));
#45795=CARTESIAN_POINT('Ctrl Pts',(178.381309917289,-4.50258461379164,336.978867064294));
#45796=CARTESIAN_POINT('Ctrl Pts',(178.373619516441,-4.4478124594802,337.103492039724));
#45797=CARTESIAN_POINT('Ctrl Pts',(178.365929115592,-4.38789630542493,337.225763622743));
#45798=CARTESIAN_POINT('Ctrl Pts',(178.358238714744,-4.32308302785332,337.345236916984));
#45799=CARTESIAN_POINT('Ctrl Pts',(178.350543892233,-4.25823248533059,337.464778903424));
#45800=CARTESIAN_POINT('Ctrl Pts',(178.342849069723,-4.18847941623002,337.581519055833));
#45801=CARTESIAN_POINT('Ctrl Pts',(178.335154247212,-4.11411436898883,337.69504100551));
#45802=CARTESIAN_POINT('Ctrl Pts',(178.32744756894,-4.03963474415269,337.808737863594));
#45803=CARTESIAN_POINT('Ctrl Pts',(178.319740890669,-3.96052918114889,337.919206292991));
#45804=CARTESIAN_POINT('Ctrl Pts',(178.312034212397,-3.8771292477966,338.026062104184));
#45805=CARTESIAN_POINT('Ctrl Pts',(178.306600851894,-3.81833064639821,338.101397563062));
#45806=CARTESIAN_POINT('Ctrl Pts',(178.301167491391,-3.75739835439175,338.174938069751));
#45807=CARTESIAN_POINT('Ctrl Pts',(178.295734130888,-3.69445924923038,338.246560321059));
#45808=CARTESIAN_POINT('Ctrl Pts',(178.287959052102,-3.60439408585605,338.349050970533));
#45809=CARTESIAN_POINT('Ctrl Pts',(178.280183973316,-3.50991847046176,338.447952891543));
#45810=CARTESIAN_POINT('Ctrl Pts',(178.27240889453,-3.41134951540899,338.542862902544));
#45811=CARTESIAN_POINT('Ctrl Pts',(178.264643383473,-3.31290185572934,338.637656120734));
#45812=CARTESIAN_POINT('Ctrl Pts',(178.256877872416,-3.21037115768049,338.72846693446));
#45813=CARTESIAN_POINT('Ctrl Pts',(178.24911236136,-3.10411439888144,338.814925538088));
#45814=CARTESIAN_POINT('Ctrl Pts',(178.24135454983,-2.9979629939665,338.90129841776));
#45815=CARTESIAN_POINT('Ctrl Pts',(178.2335967383,-2.88809318160164,338.983327429775));
#45816=CARTESIAN_POINT('Ctrl Pts',(178.225838926769,-2.77489809983399,339.060680189086));
#45817=CARTESIAN_POINT('Ctrl Pts',(178.218086953239,-2.66178820095424,339.137974737994));
#45818=CARTESIAN_POINT('Ctrl Pts',(178.210334979708,-2.54535833493829,339.210599819007));
#45819=CARTESIAN_POINT('Ctrl Pts',(178.202583006177,-2.42603368200257,339.278264091461));
#45820=CARTESIAN_POINT('Ctrl Pts',(178.194834315611,-2.3067595631265,339.345899708057));
#45821=CARTESIAN_POINT('Ctrl Pts',(178.187085625045,-2.18459343495103,339.40857850224));
#45822=CARTESIAN_POINT('Ctrl Pts',(178.17933693448,-2.05998815984202,339.466053273732));
#45823=CARTESIAN_POINT('Ctrl Pts',(178.171589856094,-1.93540880990023,339.523516087118));
#45824=CARTESIAN_POINT('Ctrl Pts',(178.163842777708,-1.80839167716165,339.575776867847));
#45825=CARTESIAN_POINT('Ctrl Pts',(178.156095699322,-1.67941248940075,339.622635260644));
#45826=CARTESIAN_POINT('Ctrl Pts',(178.148348556008,-1.55043222066922,339.669494046159));
#45827=CARTESIAN_POINT('Ctrl Pts',(178.140601412694,-1.41949023149725,339.710950219963));
#45828=CARTESIAN_POINT('Ctrl Pts',(178.13285426938,-1.28708003305147,339.746852436196));
#45829=CARTESIAN_POINT('Ctrl Pts',(178.125105384344,-1.15464006598175,339.78276272401));
#45830=CARTESIAN_POINT('Ctrl Pts',(178.117356499308,-1.02073160998556,339.813116467314));
#45831=CARTESIAN_POINT('Ctrl Pts',(178.109607614271,-0.885860672215242,
339.837812928579));
#45832=CARTESIAN_POINT('Ctrl Pts',(178.101850504489,-0.750846581037659,
339.862535602922));
#45833=CARTESIAN_POINT('Ctrl Pts',(178.094093394706,-0.614868352456746,
339.881588929765));
#45834=CARTESIAN_POINT('Ctrl Pts',(178.086336284923,-0.478440016111392,
339.894923718863));
#45835=CARTESIAN_POINT('Ctrl Pts',(178.078575029988,-0.341938776824875,
339.908265633645));
#45836=CARTESIAN_POINT('Ctrl Pts',(178.070813775054,-0.204987340582888,
339.915882900022));
#45837=CARTESIAN_POINT('Ctrl Pts',(178.06305252012,-0.0681011076885268,
339.917778492534));
#45838=CARTESIAN_POINT('Ctrl Pts',(178.055278849707,0.0690040985662645,
339.919677117377));
#45839=CARTESIAN_POINT('Ctrl Pts',(178.047505179294,0.206043502116605,339.915835789281));
#45840=CARTESIAN_POINT('Ctrl Pts',(178.039731508881,0.342504561618265,339.906309579284));
#45841=CARTESIAN_POINT('Ctrl Pts',(178.032319704792,0.472613324282115,339.897226816772));
#45842=CARTESIAN_POINT('Ctrl Pts',(178.024907900704,0.60219608894837,339.882976555734));
#45843=CARTESIAN_POINT('Ctrl Pts',(178.017496096615,0.73081794824608,339.863649677868));
#45844=CARTESIAN_POINT('Ctrl Pts',(178.009721017839,0.865743949582712,339.843375531909));
#45845=CARTESIAN_POINT('Ctrl Pts',(178.001945939062,1.0000388612588,339.817450475875));
#45846=CARTESIAN_POINT('Ctrl Pts',(177.994170860286,1.13319203161789,339.785922991647));
#45847=CARTESIAN_POINT('Ctrl Pts',(177.986405349239,1.26618134852352,339.754434303996));
#45848=CARTESIAN_POINT('Ctrl Pts',(177.978639838193,1.39803134290858,339.717356994719));
#45849=CARTESIAN_POINT('Ctrl Pts',(177.970874327146,1.5282378562543,339.674791130865));
#45850=CARTESIAN_POINT('Ctrl Pts',(177.963116515626,1.6583152694632,339.632267471188));
#45851=CARTESIAN_POINT('Ctrl Pts',(177.955358704106,1.7867520753299,339.58426620733));
#45852=CARTESIAN_POINT('Ctrl Pts',(177.947600892586,1.91305601462299,339.53093806484));
#45853=CARTESIAN_POINT('Ctrl Pts',(177.939848919065,2.03926490619641,339.477650053468));
#45854=CARTESIAN_POINT('Ctrl Pts',(177.932096945544,2.1633437673262,339.419043293903));
#45855=CARTESIAN_POINT('Ctrl Pts',(177.924344972023,2.28481751402039,339.355317668107));
#45856=CARTESIAN_POINT('Ctrl Pts',(177.916596281468,2.40623981651021,339.291619030152));
#45857=CARTESIAN_POINT('Ctrl Pts',(177.908847590913,2.52505885347051,339.222806018859));
#45858=CARTESIAN_POINT('Ctrl Pts',(177.901098900357,2.64082167910272,339.149125681596));
#45859=CARTESIAN_POINT('Ctrl Pts',(177.893351821982,2.75656041931198,339.075460674144));
#45860=CARTESIAN_POINT('Ctrl Pts',(177.885604743606,2.86924388344247,338.996930564775));
#45861=CARTESIAN_POINT('Ctrl Pts',(177.87785766523,2.97844614487324,338.913826979389));
#45862=CARTESIAN_POINT('Ctrl Pts',(177.870110521927,3.08764932152388,338.830722697514));
#45863=CARTESIAN_POINT('Ctrl Pts',(177.862363378623,3.19337092623292,338.743045099879));
#45864=CARTESIAN_POINT('Ctrl Pts',(177.85461623532,3.29521662182914,338.651127288622));
#45865=CARTESIAN_POINT('Ctrl Pts',(177.846867350294,3.3970852145003,338.559188812289));
#45866=CARTESIAN_POINT('Ctrl Pts',(177.839118465268,3.49507587398259,338.463008487228));
#45867=CARTESIAN_POINT('Ctrl Pts',(177.831369580242,3.5888300584333,338.362957310788));
#45868=CARTESIAN_POINT('Ctrl Pts',(177.82361247047,3.68268375454419,338.262799938996));
#45869=CARTESIAN_POINT('Ctrl Pts',(177.815855360697,3.7722917254758,338.158763794259));
#45870=CARTESIAN_POINT('Ctrl Pts',(177.808098250925,3.85733443517002,338.0512545154));
#45871=CARTESIAN_POINT('Ctrl Pts',(177.800336996001,3.94242258896909,337.943687787021));
#45872=CARTESIAN_POINT('Ctrl Pts',(177.792575741077,4.02294039121272,337.83264454269));
#45873=CARTESIAN_POINT('Ctrl Pts',(177.784814486153,4.09861143057847,337.71855980321));
#45874=CARTESIAN_POINT('Ctrl Pts',(177.77704081575,4.17440351894647,337.604292565327));
#45875=CARTESIAN_POINT('Ctrl Pts',(177.769267145348,4.24533314882702,337.486974444453));
#45876=CARTESIAN_POINT('Ctrl Pts',(177.761493474945,4.31116926509982,337.367066249634));
#45877=CARTESIAN_POINT('Ctrl Pts',(177.754081670744,4.37394069454455,337.252739809726));
#45878=CARTESIAN_POINT('Ctrl Pts',(177.746669866542,4.43208201639745,337.136059262717));
#45879=CARTESIAN_POINT('Ctrl Pts',(177.739258062341,4.48543430167461,337.017439512813));
#45880=CARTESIAN_POINT('Ctrl Pts',(177.731482983563,4.54140154119123,336.89300585604));
#45881=CARTESIAN_POINT('Ctrl Pts',(177.723707904786,4.59227529104021,336.766044864336));
#45882=CARTESIAN_POINT('Ctrl Pts',(177.715932826008,4.63781997775631,336.637012191899));
#45883=CARTESIAN_POINT('Ctrl Pts',(177.70816731496,4.68330861883573,336.50813830238));
#45884=CARTESIAN_POINT('Ctrl Pts',(177.700401803912,4.72348111597075,336.377198169639));
#45885=CARTESIAN_POINT('Ctrl Pts',(177.692636292864,4.75814878857253,336.24466990335));
#45886=CARTESIAN_POINT('Ctrl Pts',(177.684878481343,4.79278208807592,336.112273039224));
#45887=CARTESIAN_POINT('Ctrl Pts',(177.677120669822,4.8219213265913,335.978291550884));
#45888=CARTESIAN_POINT('Ctrl Pts',(177.6693628583,4.8454268627324,335.843220955866));
#45889=CARTESIAN_POINT('Ctrl Pts',(177.661610884778,4.86891471021218,335.708252005753));
#45890=CARTESIAN_POINT('Ctrl Pts',(177.653858911256,4.88677722716964,335.572195963845));
#45891=CARTESIAN_POINT('Ctrl Pts',(177.646106937734,4.89892540340302,335.435560506006));
#45892=CARTESIAN_POINT('Ctrl Pts',(177.638358247178,4.9110684348765,335.298982913366));
#45893=CARTESIAN_POINT('Ctrl Pts',(177.630609556621,4.91750190434473,335.161826781371));
#45894=CARTESIAN_POINT('Ctrl Pts',(177.622860866064,4.91818844424897,335.024606693316));
#45895=CARTESIAN_POINT('Ctrl Pts',(177.615113787687,4.91887484131284,334.887415155045));
#45896=CARTESIAN_POINT('Ctrl Pts',(177.607366709311,4.91381668518364,334.750160077805));
#45897=CARTESIAN_POINT('Ctrl Pts',(177.599619630934,4.90302871696604,334.613357447885));
#45898=CARTESIAN_POINT('Ctrl Pts',(177.591872487629,4.89224065833493,334.476553671427));
#45899=CARTESIAN_POINT('Ctrl Pts',(177.584125344324,4.87572272256143,334.340202739516));
#45900=CARTESIAN_POINT('Ctrl Pts',(177.576378201019,4.85354162387011,334.204816519374));
#45901=CARTESIAN_POINT('Ctrl Pts',(177.568629315992,4.83135553839694,334.069399861536));
#45902=CARTESIAN_POINT('Ctrl Pts',(177.560880430965,4.80350381966597,333.934948732704));
#45903=CARTESIAN_POINT('Ctrl Pts',(177.553131545938,4.77010441969993,333.801965406318));
#45904=CARTESIAN_POINT('Ctrl Pts',(177.545374436164,4.73666956926564,333.668840930055));
#45905=CARTESIAN_POINT('Ctrl Pts',(177.537617326391,4.69767537039572,333.53718774807));
#45906=CARTESIAN_POINT('Ctrl Pts',(177.529860216617,4.65329001413586,333.407494079495));
#45907=CARTESIAN_POINT('Ctrl Pts',(177.522098961692,4.60888093976079,333.27773110677));
#45908=CARTESIAN_POINT('Ctrl Pts',(177.514337706767,4.55907510947838,333.149930097909));
#45909=CARTESIAN_POINT('Ctrl Pts',(177.506576451842,4.50408875953656,333.024558907809));
#45910=CARTESIAN_POINT('Ctrl Pts',(177.498802781438,4.44901444935495,332.898987164663));
#45911=CARTESIAN_POINT('Ctrl Pts',(177.491029111034,4.38874323128088,332.77585335875));
#45912=CARTESIAN_POINT('Ctrl Pts',(177.483255440631,4.32353757229044,332.655601159467));
#45913=CARTESIAN_POINT('Ctrl Pts',(177.475843636443,4.26136725231417,332.540946728808));
#45914=CARTESIAN_POINT('Ctrl Pts',(177.468431832255,4.19471169657706,332.428911911962));
#45915=CARTESIAN_POINT('Ctrl Pts',(177.461020028067,4.12383380128391,332.319854884174));
#45916=CARTESIAN_POINT('Ctrl Pts',(177.453244949287,4.04948196930619,332.20545264674));
#45917=CARTESIAN_POINT('Ctrl Pts',(177.445469870508,3.97024846794033,332.093965947486));
#45918=CARTESIAN_POINT('Ctrl Pts',(177.437694791728,3.88638898420485,331.985839465796));
#45919=CARTESIAN_POINT('Ctrl Pts',(177.429929280678,3.80263269490266,331.877846040626));
#45920=CARTESIAN_POINT('Ctrl Pts',(177.422163769628,3.71426198706275,331.773204911548));
#45921=CARTESIAN_POINT('Ctrl Pts',(177.414398258578,3.62157680741814,331.672333476673));
#45922=CARTESIAN_POINT('Ctrl Pts',(177.406640447055,3.52898352539915,331.57156205612));
#45923=CARTESIAN_POINT('Ctrl Pts',(177.398882635531,3.43208454742217,331.474553177578));
#45924=CARTESIAN_POINT('Ctrl Pts',(177.391124824008,3.33122099678566,331.381692421439));
#45925=CARTESIAN_POINT('Ctrl Pts',(177.383372850484,3.23043334916917,331.288901545963));
#45926=CARTESIAN_POINT('Ctrl Pts',(177.37562087696,3.12568735374209,331.200252843189));
#45927=CARTESIAN_POINT('Ctrl Pts',(177.367868903435,3.01736175744166,331.116095896237));
#45928=CARTESIAN_POINT('Ctrl Pts',(177.360120212877,2.90908203709536,331.031974589801));
#45929=CARTESIAN_POINT('Ctrl Pts',(177.352371522318,2.79722603904751,330.952341495026));
#45930=CARTESIAN_POINT('Ctrl Pts',(177.344622831759,2.68220626563671,330.877506505635));
#45931=CARTESIAN_POINT('Ctrl Pts',(177.33687575338,2.56721042305009,330.802687086289));
#45932=CARTESIAN_POINT('Ctrl Pts',(177.329128675001,2.44905244183251,330.732663999698));
#45933=CARTESIAN_POINT('Ctrl Pts',(177.321381596622,2.3281742031205,330.667704079541));
#45934=CARTESIAN_POINT('Ctrl Pts',(177.313634453315,2.20729495133221,330.602743614958));
#45935=CARTESIAN_POINT('Ctrl Pts',(177.305887310008,2.08369574088242,330.542846586477));
#45936=CARTESIAN_POINT('Ctrl Pts',(177.298140166701,1.95784311473272,330.488233893408));
#45937=CARTESIAN_POINT('Ctrl Pts',(177.290391281671,1.83196219424135,330.433608922246));
#45938=CARTESIAN_POINT('Ctrl Pts',(177.282642396642,1.70382720844067,330.384270806113));
#45939=CARTESIAN_POINT('Ctrl Pts',(177.274893511613,1.57392436038893,330.340392165614));
#45940=CARTESIAN_POINT('Ctrl Pts',(177.267136401837,1.44388363211172,330.296466951872));
#45941=CARTESIAN_POINT('Ctrl Pts',(177.259379292061,1.31207166414775,330.258012914593));
#45942=CARTESIAN_POINT('Ctrl Pts',(177.251622182285,1.17899002820679,330.225152821724));
#45943=CARTESIAN_POINT('Ctrl Pts',(177.243860927358,1.04583727769469,330.192275169473));
#45944=CARTESIAN_POINT('Ctrl Pts',(177.23609967243,0.911413890165617,330.164997495625));
#45945=CARTESIAN_POINT('Ctrl Pts',(177.228338417503,0.776230312625155,330.143391145639));
#45946=CARTESIAN_POINT('Ctrl Pts',(177.220564747097,0.640830485416796,330.121750232533));
#45947=CARTESIAN_POINT('Ctrl Pts',(177.212791076691,0.504668426580055,330.105798817874));
#45948=CARTESIAN_POINT('Ctrl Pts',(177.205017406285,0.368259263117793,330.095556282551));
#45949=CARTESIAN_POINT('Ctrl Pts',(177.197605602121,0.238199979280686,330.085790539729));
#45950=CARTESIAN_POINT('Ctrl Pts',(177.190193797957,0.107916366155344,330.081214150661));
#45951=CARTESIAN_POINT('Ctrl Pts',(177.182781993793,-0.0221481108367294,
330.081799869496));
#45952=CARTESIAN_POINT('Ctrl Pts',(177.175006915015,-0.158587435520085,
330.082414296158));
#45953=CARTESIAN_POINT('Ctrl Pts',(177.167231836237,-0.295216773365073,
330.088711587753));
#45954=CARTESIAN_POINT('Ctrl Pts',(177.159456757459,-0.431523817072754,
330.100717373145));
#45955=CARTESIAN_POINT('Ctrl Pts',(177.15169124641,-0.567663126285112,330.112708384655));
#45956=CARTESIAN_POINT('Ctrl Pts',(177.143925735362,-0.703480544842646,
330.130393878924));
#45957=CARTESIAN_POINT('Ctrl Pts',(177.136160224313,-0.83846275538047,330.153747502416));
#45958=CARTESIAN_POINT('Ctrl Pts',(177.128402412791,-0.973311130663834,
330.177077970722));
#45959=CARTESIAN_POINT('Ctrl Pts',(177.120644601269,-1.10732556324428,330.206065317992));
#45960=CARTESIAN_POINT('Ctrl Pts',(177.112886789748,-1.23999720895503,330.240631346041));
#45961=CARTESIAN_POINT('Ctrl Pts',(177.105134816225,-1.37256901504501,330.275171362058));
#45962=CARTESIAN_POINT('Ctrl Pts',(177.097382842702,-1.50379966887132,330.315281604522));
#45963=CARTESIAN_POINT('Ctrl Pts',(177.08963086918,-1.63319023683207,330.360832756537));
#45964=CARTESIAN_POINT('Ctrl Pts',(177.081882178623,-1.76252600781031,330.406364617613));
#45965=CARTESIAN_POINT('Ctrl Pts',(177.074133488065,-1.89002287492386,330.457332675765));
#45966=CARTESIAN_POINT('Ctrl Pts',(177.066384797508,-2.01519701324465,330.513557750254));
#45967=CARTESIAN_POINT('Ctrl Pts',(177.058637719131,-2.14034510804055,330.569771126646));
#45968=CARTESIAN_POINT('Ctrl Pts',(177.050890640753,-2.26317107895541,330.631239183739));
#45969=CARTESIAN_POINT('Ctrl Pts',(177.043143562376,-2.38321141261797,330.697734733275));
#45970=CARTESIAN_POINT('Ctrl Pts',(177.03539641907,-2.50325275233455,330.764230840108));
#45971=CARTESIAN_POINT('Ctrl Pts',(177.027649275765,-2.62050806631345,330.83575433402));
#45972=CARTESIAN_POINT('Ctrl Pts',(177.01990213246,-2.7345391224461,330.912032430374));
#45973=CARTESIAN_POINT('Ctrl Pts',(177.012153247432,-2.84859581518041,330.988327675663));
#45974=CARTESIAN_POINT('Ctrl Pts',(177.004404362404,-2.95942648281034,331.069379433174));
#45975=CARTESIAN_POINT('Ctrl Pts',(176.996655477376,-3.06662285261261,331.154872259296));
#45976=CARTESIAN_POINT('Ctrl Pts',(176.988898367602,-3.17393300174964,331.240455828387));
#45977=CARTESIAN_POINT('Ctrl Pts',(176.981141257828,-3.27760084130692,331.330489638237));
#45978=CARTESIAN_POINT('Ctrl Pts',(176.973384148053,-3.37725170386577,331.424618343276));
#45979=CARTESIAN_POINT('Ctrl Pts',(176.965622893128,-3.47695581665924,331.518797347686));
#45980=CARTESIAN_POINT('Ctrl Pts',(176.957861638202,-3.57263840274313,331.617075327511));
#45981=CARTESIAN_POINT('Ctrl Pts',(176.950100383276,-3.66396323403733,331.719061646095));
#45982=CARTESIAN_POINT('Ctrl Pts',(176.942326712872,-3.75543415529907,331.821211109552));
#45983=CARTESIAN_POINT('Ctrl Pts',(176.934553042468,-3.84253314321025,331.927080463919));
#45984=CARTESIAN_POINT('Ctrl Pts',(176.926779372063,-3.92496513518874,332.03624701602));
#45985=CARTESIAN_POINT('Ctrl Pts',(176.919367567882,-4.00355989815917,332.140331838923));
#45986=CARTESIAN_POINT('Ctrl Pts',(176.9119557637,-4.07791222027853,332.247413562207));
#45987=CARTESIAN_POINT('Ctrl Pts',(176.904543959519,-4.14780502857619,332.357104522041));
#45988=CARTESIAN_POINT('Ctrl Pts',(176.896578469935,-4.22291905248635,332.474989746292));
#45989=CARTESIAN_POINT('Ctrl Pts',(176.88861298035,-4.29311033714613,332.596246708684));
#45990=CARTESIAN_POINT('Ctrl Pts',(176.880647490766,-4.35807046888413,332.720437574722));
#45991=CARTESIAN_POINT('Ctrl Pts',(176.872693252424,-4.42293884453604,332.844453021352));
#45992=CARTESIAN_POINT('Ctrl Pts',(176.864739014081,-4.48259061177193,332.97139379955));
#45993=CARTESIAN_POINT('Ctrl Pts',(176.856784775739,-4.53676066080434,333.100793384311));
#45994=CARTESIAN_POINT('Ctrl Pts',(176.848840386968,-4.59086363216895,333.230032736202));
#45995=CARTESIAN_POINT('Ctrl Pts',(176.840895998197,-4.63949826263529,333.361724496742));
#45996=CARTESIAN_POINT('Ctrl Pts',(176.832951609425,-4.68244544840857,333.495377892899));
#45997=CARTESIAN_POINT('Ctrl Pts',(176.825017922654,-4.72533477941262,333.62885124265));
#45998=CARTESIAN_POINT('Ctrl Pts',(176.817084235883,-4.76255182620758,333.764280614637));
#45999=CARTESIAN_POINT('Ctrl Pts',(176.809150549112,-4.79392586400262,333.901156119848));
#46000=CARTESIAN_POINT('Ctrl Pts',(176.801223146645,-4.82527505029799,334.037923205429));
#46001=CARTESIAN_POINT('Ctrl Pts',(176.793295744179,-4.85079036196863,334.176133788734));
#46002=CARTESIAN_POINT('Ctrl Pts',(176.785368341712,-4.8703509690766,334.315263188871));
#46003=CARTESIAN_POINT('Ctrl Pts',(176.777446779236,-4.88989716619812,334.454290094604));
#46004=CARTESIAN_POINT('Ctrl Pts',(176.769525216761,-4.90349734986709,334.594234107436));
#46005=CARTESIAN_POINT('Ctrl Pts',(176.761603654285,-4.91108187582924,334.734560983649));
#46006=CARTESIAN_POINT('Ctrl Pts',(176.756581185687,-4.91589065485409,334.823531730446));
#46007=CARTESIAN_POINT('Ctrl Pts',(176.751558717088,-4.91828224055931,334.912656185423));
#46008=CARTESIAN_POINT('Ctrl Pts',(176.74653624849,-4.91824967172928,335.001796951547));
#46009=CARTESIAN_POINT('',(180.24653624852,-4.91824998793836,335.000344447839));
#46010=CARTESIAN_POINT('Ctrl Pts',(180.24653624849,-4.91824998793832,335.000344448365));
#46011=CARTESIAN_POINT('Ctrl Pts',(180.245490955929,-4.9182487032425,335.018688141735));
#46012=CARTESIAN_POINT('Ctrl Pts',(180.244445663368,-4.91814479377736,335.037031417793));
#46013=CARTESIAN_POINT('Ctrl Pts',(180.243400370807,-4.91793827065545,335.055373536301));
#46014=CARTESIAN_POINT('Ctrl Pts',(180.235625292529,-4.91640211369949,335.191805586485));
#46015=CARTESIAN_POINT('Ctrl Pts',(180.227850214252,-4.90918193865282,335.328389254008));
#46016=CARTESIAN_POINT('Ctrl Pts',(180.220075135975,-4.89625557816743,335.464612070188));
#46017=CARTESIAN_POINT('Ctrl Pts',(180.212309625435,-4.88334512440573,335.60066725537));
#46018=CARTESIAN_POINT('Ctrl Pts',(180.204544114896,-4.86474249320673,335.736362087336));
#46019=CARTESIAN_POINT('Ctrl Pts',(180.196778604356,-4.84047750526045,335.871183438529));
#46020=CARTESIAN_POINT('Ctrl Pts',(180.18902079335,-4.81623657614479,336.005871113824));
#46021=CARTESIAN_POINT('Ctrl Pts',(180.181262982344,-4.78634453174525,336.139686649638));
#46022=CARTESIAN_POINT('Ctrl Pts',(180.173505171339,-4.75088300599652,336.27212174175));
#46023=CARTESIAN_POINT('Ctrl Pts',(180.165753198339,-4.71544816620316,336.404457172133));
#46024=CARTESIAN_POINT('Ctrl Pts',(180.158001225339,-4.67445228816595,336.5354138505));
#46025=CARTESIAN_POINT('Ctrl Pts',(180.15024925234,-4.62802805641185,336.664493728304));
#46026=CARTESIAN_POINT('Ctrl Pts',(180.142500562314,-4.58162348539915,336.79351894056));
#46027=CARTESIAN_POINT('Ctrl Pts',(180.134751872288,-4.52979526506278,336.920668566067));
#46028=CARTESIAN_POINT('Ctrl Pts',(180.127003182262,-4.47272584056937,337.045460001467));
#46029=CARTESIAN_POINT('Ctrl Pts',(180.119256104421,-4.41566828988442,337.170225472885));
#46030=CARTESIAN_POINT('Ctrl Pts',(180.11150902658,-4.35337186654326,337.292633374876));
#46031=CARTESIAN_POINT('Ctrl Pts',(180.103761948739,-4.28606688491897,337.412221739497));
#46032=CARTESIAN_POINT('Ctrl Pts',(180.096014805974,-4.21876133925372,337.531811106313));
#46033=CARTESIAN_POINT('Ctrl Pts',(180.08826766321,-4.14644734329543,337.648580547998));
#46034=CARTESIAN_POINT('Ctrl Pts',(180.080520520445,-4.06940063596396,337.762093685326));
#46035=CARTESIAN_POINT('Ctrl Pts',(180.072771635962,-3.99233660693642,337.875632342758));
#46036=CARTESIAN_POINT('Ctrl Pts',(180.06502275148,-3.91053796874405,337.985912915717));
#46037=CARTESIAN_POINT('Ctrl Pts',(180.057273866997,-3.82432291591003,338.092529271866));
#46038=CARTESIAN_POINT('Ctrl Pts',(180.049516757771,-3.73801635355931,338.199258791678));
#46039=CARTESIAN_POINT('Ctrl Pts',(180.041759648545,-3.64728425875788,338.30231602115));
#46040=CARTESIAN_POINT('Ctrl Pts',(180.034002539319,-3.5524845000535,338.401328702049));
#46041=CARTESIAN_POINT('Ctrl Pts',(180.026241284944,-3.45763408341873,338.500394292127));
#46042=CARTESIAN_POINT('Ctrl Pts',(180.01848003057,-3.35871195348679,338.595410756462));
#46043=CARTESIAN_POINT('Ctrl Pts',(180.010718776195,-3.25611100940342,338.686044513695));
#46044=CARTESIAN_POINT('Ctrl Pts',(180.002945106341,-3.15334593722364,338.776823255423));
#46045=CARTESIAN_POINT('Ctrl Pts',(179.995171436487,-3.04689059479092,338.863205033769));
#46046=CARTESIAN_POINT('Ctrl Pts',(179.987397766633,-2.93716965893771,338.944897648497));
#46047=CARTESIAN_POINT('Ctrl Pts',(179.979985956599,-2.83255616897477,339.022787519417));
#46048=CARTESIAN_POINT('Ctrl Pts',(179.972574146566,-2.72497450279379,339.096414793428));
#46049=CARTESIAN_POINT('Ctrl Pts',(179.965162336532,-2.6148137828259,339.165565020936));
#46050=CARTESIAN_POINT('Ctrl Pts',(179.95738725742,-2.49925384417118,339.238104452878));
#46051=CARTESIAN_POINT('Ctrl Pts',(179.949612178308,-2.38049045859568,339.305946120166));
#46052=CARTESIAN_POINT('Ctrl Pts',(179.941837099196,-2.25894257607548,339.368794055628));
#46053=CARTESIAN_POINT('Ctrl Pts',(179.934071587809,-2.1375442658974,339.431564652739));
#46054=CARTESIAN_POINT('Ctrl Pts',(179.926306076423,-2.01336862041317,339.489353567204));
#46055=CARTESIAN_POINT('Ctrl Pts',(179.918540565036,-1.88686327735886,339.541908193156));
#46056=CARTESIAN_POINT('Ctrl Pts',(179.910782753173,-1.76048336465994,339.594410711068));
#46057=CARTESIAN_POINT('Ctrl Pts',(179.90302494131,-1.63177870986369,339.641689119491));
#46058=CARTESIAN_POINT('Ctrl Pts',(179.895267129447,-1.50122093376931,339.68353699361));
#46059=CARTESIAN_POINT('Ctrl Pts',(179.88751515558,-1.37076140648656,339.725353375894));
#46060=CARTESIAN_POINT('Ctrl Pts',(179.879763181713,-1.23845190437485,339.761747239317));
#46061=CARTESIAN_POINT('Ctrl Pts',(179.872011207846,-1.10478305041207,339.792560638534));
#46062=CARTESIAN_POINT('Ctrl Pts',(179.864262516941,-0.971170805227721,
339.823360988272));
#46063=CARTESIAN_POINT('Ctrl Pts',(179.856513826036,-0.836200733283099,
339.848585486676));
#46064=CARTESIAN_POINT('Ctrl Pts',(179.848765135131,-0.700377397695667,
339.868126391467));
#46065=CARTESIAN_POINT('Ctrl Pts',(179.841018056404,-0.564582321251315,
339.887663230614));
#46066=CARTESIAN_POINT('Ctrl Pts',(179.833270977677,-0.427934720928508,
339.901518772632));
#46067=CARTESIAN_POINT('Ctrl Pts',(179.82552389895,-0.290947711851586,339.909636696485));
#46068=CARTESIAN_POINT('Ctrl Pts',(179.817776755293,-0.153959554662009,
339.917754688375));
#46069=CARTESIAN_POINT('Ctrl Pts',(179.810029611637,-0.0166323732341754,
339.920134943061));
#46070=CARTESIAN_POINT('Ctrl Pts',(179.80228246798,0.120517653584459,339.916773185502));
#46071=CARTESIAN_POINT('Ctrl Pts',(179.7945335826,0.257698514663268,339.913410672148));
#46072=CARTESIAN_POINT('Ctrl Pts',(179.786784697219,0.394701751198794,339.904303587325));
#46073=CARTESIAN_POINT('Ctrl Pts',(179.779035811839,0.531013644441538,339.889499726139));
#46074=CARTESIAN_POINT('Ctrl Pts',(179.771278701712,0.667470220532111,339.874680151983));
#46075=CARTESIAN_POINT('Ctrl Pts',(179.763521591584,0.803233598294663,339.854151765049));
#46076=CARTESIAN_POINT('Ctrl Pts',(179.755764481457,0.937797074547684,339.828014054399));
#46077=CARTESIAN_POINT('Ctrl Pts',(179.748003226178,1.07243245722768,339.80186237659));
#46078=CARTESIAN_POINT('Ctrl Pts',(179.740241970899,1.20586628071717,339.770095492868));
#46079=CARTESIAN_POINT('Ctrl Pts',(179.73248071562,1.3376054089815,339.732863280548));
#46080=CARTESIAN_POINT('Ctrl Pts',(179.724707044864,1.46955527686569,339.695571508838));
#46081=CARTESIAN_POINT('Ctrl Pts',(179.716933374109,1.59980466066831,339.652797059961));
#46082=CARTESIAN_POINT('Ctrl Pts',(179.709159703354,1.72787802589608,339.604738927467));
#46083=CARTESIAN_POINT('Ctrl Pts',(179.701747902989,1.84998947685191,339.558917938233));
#46084=CARTESIAN_POINT('Ctrl Pts',(179.694336102623,1.97012267446546,339.508294223313));
#46085=CARTESIAN_POINT('Ctrl Pts',(179.686924302258,2.0878867086058,339.4530789522));
#46086=CARTESIAN_POINT('Ctrl Pts',(179.67914922353,2.21142277158844,339.395157386761));
#46087=CARTESIAN_POINT('Ctrl Pts',(179.671374144803,2.3327419534251,339.331999744926));
#46088=CARTESIAN_POINT('Ctrl Pts',(179.663599066075,2.4513686511619,339.263798165791));
#46089=CARTESIAN_POINT('Ctrl Pts',(179.655833555076,2.56984937119489,339.19568051304));
#46090=CARTESIAN_POINT('Ctrl Pts',(179.648068044078,2.68564386396864,339.12253146587));
#46091=CARTESIAN_POINT('Ctrl Pts',(179.64030253308,2.79829746537685,339.044590752816));
#46092=CARTESIAN_POINT('Ctrl Pts',(179.632544721608,2.91083937041216,338.966727318205));
#46093=CARTESIAN_POINT('Ctrl Pts',(179.624786910136,3.02024626215157,338.884081893331));
#46094=CARTESIAN_POINT('Ctrl Pts',(179.617029098665,3.12608933250522,338.796939365818));
#46095=CARTESIAN_POINT('Ctrl Pts',(179.609277125192,3.23185275259354,338.709862415819));
#46096=CARTESIAN_POINT('Ctrl Pts',(179.601525151719,3.33405738892024,338.618295346733));
#46097=CARTESIAN_POINT('Ctrl Pts',(179.593773178247,3.43230491764391,338.522565260548));
#46098=CARTESIAN_POINT('Ctrl Pts',(179.586024487739,3.53051083848612,338.426875716106));
#46099=CARTESIAN_POINT('Ctrl Pts',(179.578275797231,3.62476270547678,338.327026933339));
#46100=CARTESIAN_POINT('Ctrl Pts',(179.570527106724,3.71469686779026,338.223384904558));
#46101=CARTESIAN_POINT('Ctrl Pts',(179.562780028395,3.80461231855318,338.119764439362));
#46102=CARTESIAN_POINT('Ctrl Pts',(179.555032950067,3.89021159547421,338.012352592995));
#46103=CARTESIAN_POINT('Ctrl Pts',(179.547285871739,3.97116966096564,337.901550376321));
#46104=CARTESIAN_POINT('Ctrl Pts',(179.539538728483,4.05212840496694,337.790747231012));
#46105=CARTESIAN_POINT('Ctrl Pts',(179.531791585226,4.12844562935505,337.676553974325));
#46106=CARTESIAN_POINT('Ctrl Pts',(179.52404444197,4.19983840517142,337.559402358549));
#46107=CARTESIAN_POINT('Ctrl Pts',(179.51629555699,4.27124723160302,337.442224404597));
#46108=CARTESIAN_POINT('Ctrl Pts',(179.508546672011,4.33772920304924,337.32208710179));
#46109=CARTESIAN_POINT('Ctrl Pts',(179.500797787032,4.39904650875091,337.199448311815));
#46110=CARTESIAN_POINT('Ctrl Pts',(179.493040677306,4.46042889728169,337.076679351747));
#46111=CARTESIAN_POINT('Ctrl Pts',(179.485283567579,4.5166354945222,336.951403950854));
#46112=CARTESIAN_POINT('Ctrl Pts',(179.477526457852,4.56747575678702,336.824102045847));
#46113=CARTESIAN_POINT('Ctrl Pts',(179.469765202974,4.61834318646519,336.696732114765));
#46114=CARTESIAN_POINT('Ctrl Pts',(179.462003948095,4.66383843763788,336.567333890356));
#46115=CARTESIAN_POINT('Ctrl Pts',(179.454242693217,4.70382068113828,336.436403168402));
#46116=CARTESIAN_POINT('Ctrl Pts',(179.446469022859,4.74386688320451,336.305262999943));
#46117=CARTESIAN_POINT('Ctrl Pts',(179.438695352501,4.77838235613106,336.172585813604));
#46118=CARTESIAN_POINT('Ctrl Pts',(179.430921682143,4.80727709884326,336.038879183273));
#46119=CARTESIAN_POINT('Ctrl Pts',(179.423509877423,4.83482678651144,335.911396618659));
#46120=CARTESIAN_POINT('Ctrl Pts',(179.416098072704,4.8572672072836,335.782978577792));
#46121=CARTESIAN_POINT('Ctrl Pts',(179.408686267984,4.87456439414474,335.654068062083));
#46122=CARTESIAN_POINT('Ctrl Pts',(179.40091118927,4.89270936618117,335.518839269012));
#46123=CARTESIAN_POINT('Ctrl Pts',(179.393136110556,4.9052515283151,335.382641157187));
#46124=CARTESIAN_POINT('Ctrl Pts',(179.385361031843,4.91209507835586,335.245977648765));
#46125=CARTESIAN_POINT('Ctrl Pts',(179.377595520859,4.91893020697159,335.109482313511));
#46126=CARTESIAN_POINT('Ctrl Pts',(179.369830009876,4.920080657008,334.972523107822));
#46127=CARTESIAN_POINT('Ctrl Pts',(179.362064498892,4.91550197646241,334.835612099307));
#46128=CARTESIAN_POINT('Ctrl Pts',(179.354306687437,4.91092783569256,334.698836838475));
#46129=CARTESIAN_POINT('Ctrl Pts',(179.346548875981,4.90063588173872,334.562110067858));
#46130=CARTESIAN_POINT('Ctrl Pts',(179.338791064526,4.88463363001364,334.425946550363));
#46131=CARTESIAN_POINT('Ctrl Pts',(179.33103909107,4.86864342049248,334.289885500251));
#46132=CARTESIAN_POINT('Ctrl Pts',(179.323287117615,4.84695151196733,334.154387246218));
#46133=CARTESIAN_POINT('Ctrl Pts',(179.31553514416,4.81961741558545,334.019963760933));
#46134=CARTESIAN_POINT('Ctrl Pts',(179.307786453671,4.79229489521391,333.885597204094));
#46135=CARTESIAN_POINT('Ctrl Pts',(179.300037763182,4.75933501720027,333.75230489295));
#46136=CARTESIAN_POINT('Ctrl Pts',(179.292289072693,4.72084875995142,333.620590688677));
#46137=CARTESIAN_POINT('Ctrl Pts',(179.284541994385,4.68237051009347,333.488903888656));
#46138=CARTESIAN_POINT('Ctrl Pts',(179.276794916077,4.6383682776122,333.358794917368));
#46139=CARTESIAN_POINT('Ctrl Pts',(179.269047837768,4.58900338460175,333.230754115841));
#46140=CARTESIAN_POINT('Ctrl Pts',(179.261300694533,4.53963807787014,333.10271224122));
#46141=CARTESIAN_POINT('Ctrl Pts',(179.253553551297,4.48491016157507,332.97673893564));
#46142=CARTESIAN_POINT('Ctrl Pts',(179.245806408061,4.42502959632726,332.853305766038));
#46143=CARTESIAN_POINT('Ctrl Pts',(179.238057523104,4.36513556866156,332.729844846047));
#46144=CARTESIAN_POINT('Ctrl Pts',(179.230308638147,4.30008675748139,332.608925550018));
#46145=CARTESIAN_POINT('Ctrl Pts',(179.222559753189,4.23013949539465,332.490995633323));
#46146=CARTESIAN_POINT('Ctrl Pts',(179.214802643486,4.16011799056537,332.372940544604));
#46147=CARTESIAN_POINT('Ctrl Pts',(179.207045533782,4.0851878485239,332.257881510219));
#46148=CARTESIAN_POINT('Ctrl Pts',(179.199288424079,4.00564954416337,332.146238483712));
#46149=CARTESIAN_POINT('Ctrl Pts',(179.191527169224,3.92606873707989,332.034535798748));
#46150=CARTESIAN_POINT('Ctrl Pts',(179.18376591437,3.84187510082044,331.926253067364));
#46151=CARTESIAN_POINT('Ctrl Pts',(179.176004659516,3.75340934988947,331.821777019361));
#46152=CARTESIAN_POINT('Ctrl Pts',(179.168230989183,3.66480208258636,331.717133843728));
#46153=CARTESIAN_POINT('Ctrl Pts',(179.16045731885,3.57190930926451,331.616309807623));
#46154=CARTESIAN_POINT('Ctrl Pts',(179.152683648517,3.47510915488219,331.519655272225));
#46155=CARTESIAN_POINT('Ctrl Pts',(179.145271843581,3.38281506068305,331.427500018427));
#46156=CARTESIAN_POINT('Ctrl Pts',(179.137860038646,3.28696938682149,331.339135016504));
#46157=CARTESIAN_POINT('Ctrl Pts',(179.130448233711,3.18792628116515,331.254828563556));
#46158=CARTESIAN_POINT('Ctrl Pts',(179.122673154881,3.08402878781031,331.166390008677));
#46159=CARTESIAN_POINT('Ctrl Pts',(179.114898076051,2.97628417163581,331.082138422369));
#46160=CARTESIAN_POINT('Ctrl Pts',(179.107122997222,2.8650643474924,331.002427067929));
#46161=CARTESIAN_POINT('Ctrl Pts',(179.099357486121,2.75398138641355,330.922813803378));
#46162=CARTESIAN_POINT('Ctrl Pts',(179.09159197502,2.63943204097068,330.847729879603));
#46163=CARTESIAN_POINT('Ctrl Pts',(179.083826463919,2.52182286423267,330.777489786403));
#46164=CARTESIAN_POINT('Ctrl Pts',(179.076068652345,2.40433029732672,330.707319336454));
#46165=CARTESIAN_POINT('Ctrl Pts',(179.06831084077,2.28378427004081,330.641983358621));
#46166=CARTESIAN_POINT('Ctrl Pts',(179.060553029195,2.1606217245274,330.581754100777));
#46167=CARTESIAN_POINT('Ctrl Pts',(179.05280105562,2.03755186272676,330.521570167355));
#46168=CARTESIAN_POINT('Ctrl Pts',(179.045049082044,1.91186975164524,330.466485475703));
#46169=CARTESIAN_POINT('Ctrl Pts',(179.037297108468,1.78403812493704,330.41672703941));
#46170=CARTESIAN_POINT('Ctrl Pts',(179.029548417857,1.65626063498904,330.366989675842));
#46171=CARTESIAN_POINT('Ctrl Pts',(179.021799727246,1.52633580347281,330.32257422275));
#46172=CARTESIAN_POINT('Ctrl Pts',(179.014051036635,1.39474739480084,330.283660024214));
#46173=CARTESIAN_POINT('Ctrl Pts',(179.006303958203,1.26318636419047,330.2447539221));
#46174=CARTESIAN_POINT('Ctrl Pts',(178.998556879771,1.1299628194759,330.211346908665));
#46175=CARTESIAN_POINT('Ctrl Pts',(178.99080980134,0.995576399546803,330.183568676378));
#46176=CARTESIAN_POINT('Ctrl Pts',(178.98306265798,0.861188853325156,330.155790211282));
#46177=CARTESIAN_POINT('Ctrl Pts',(178.97531551462,0.72563879523206,330.133640700551));
#46178=CARTESIAN_POINT('Ctrl Pts',(178.96756837126,0.589436397711769,330.117198775748));
#46179=CARTESIAN_POINT('Ctrl Pts',(178.959819486178,0.45320337899708,330.100753154452));
#46180=CARTESIAN_POINT('Ctrl Pts',(178.952070601095,0.316318116999823,330.090017719318));
#46181=CARTESIAN_POINT('Ctrl Pts',(178.944321716013,0.179295855061354,330.085019220907));
#46182=CARTESIAN_POINT('Ctrl Pts',(178.936564606184,0.0421281562781302,
330.080015417037));
#46183=CARTESIAN_POINT('Ctrl Pts',(178.928807496355,-0.0951764416912896,
330.080760727998));
#46184=CARTESIAN_POINT('Ctrl Pts',(178.921050386526,-0.232102186732936,
330.087229738995));
#46185=CARTESIAN_POINT('Ctrl Pts',(178.913289131545,-0.36910110051628,330.093702206825));
#46186=CARTESIAN_POINT('Ctrl Pts',(178.905527876564,-0.505720368851173,
330.105904434397));
#46187=CARTESIAN_POINT('Ctrl Pts',(178.897766621584,-0.64145040221728,330.123759189294));
#46188=CARTESIAN_POINT('Ctrl Pts',(178.889992951125,-0.777397559394959,
330.141642505979));
#46189=CARTESIAN_POINT('Ctrl Pts',(178.882219280666,-0.912452253790739,
330.165196351795));
#46190=CARTESIAN_POINT('Ctrl Pts',(178.874445610207,-1.04611523409038,330.194292353929));
#46191=CARTESIAN_POINT('Ctrl Pts',(178.867033806617,-1.17355615952385,330.222033927774));
#46192=CARTESIAN_POINT('Ctrl Pts',(178.859622003027,-1.29973174525168,330.254813221642));
#46193=CARTESIAN_POINT('Ctrl Pts',(178.852210199436,-1.42422472502374,330.292477616078));
#46194=CARTESIAN_POINT('Ctrl Pts',(178.844435120669,-1.55481948672895,330.331988057752));
#46195=CARTESIAN_POINT('Ctrl Pts',(178.836660041902,-1.68397523620287,330.376999435934));
#46196=CARTESIAN_POINT('Ctrl Pts',(178.828884963135,-1.81119364234137,330.427390170544));
#46197=CARTESIAN_POINT('Ctrl Pts',(178.821119452097,-1.93825549813117,330.477718896145));
#46198=CARTESIAN_POINT('Ctrl Pts',(178.813353941059,-2.06338439417958,330.533413664419));
#46199=CARTESIAN_POINT('Ctrl Pts',(178.805588430022,-2.18609586011521,330.594302784702));
#46200=CARTESIAN_POINT('Ctrl Pts',(178.797830618511,-2.30868565727432,330.655131533244));
#46201=CARTESIAN_POINT('Ctrl Pts',(178.790072807,-2.42886244638127,330.721144211956));
#46202=CARTESIAN_POINT('Ctrl Pts',(178.782314995489,-2.54616083392577,330.792120715814));
#46203=CARTESIAN_POINT('Ctrl Pts',(178.774563021977,-2.6633709507132,330.863043807602));
#46204=CARTESIAN_POINT('Ctrl Pts',(178.766811048466,-2.77770664435982,330.938923087794));
#46205=CARTESIAN_POINT('Ctrl Pts',(178.759059074954,-2.88872660256619,331.019492283876));
#46206=CARTESIAN_POINT('Ctrl Pts',(178.751310384408,-2.99969954375468,331.100027358855));
#46207=CARTESIAN_POINT('Ctrl Pts',(178.743561693862,-3.10735922669989,331.185248170248));
#46208=CARTESIAN_POINT('Ctrl Pts',(178.735813003315,-3.21129304446125,331.274844963616));
#46209=CARTESIAN_POINT('Ctrl Pts',(178.728065924949,-3.31520523792383,331.364423115624));
#46210=CARTESIAN_POINT('Ctrl Pts',(178.720318846582,-3.41539281225687,331.458375183585));
#46211=CARTESIAN_POINT('Ctrl Pts',(178.712571768216,-3.51147632302539,331.556351194542));
#46212=CARTESIAN_POINT('Ctrl Pts',(178.704824624921,-3.60756063906641,331.654328026633));
#46213=CARTESIAN_POINT('Ctrl Pts',(178.697077481627,-3.69954054925603,331.756328589914));
#46214=CARTESIAN_POINT('Ctrl Pts',(178.689330338332,-3.78707384705354,331.861966421553));
#46215=CARTESIAN_POINT('Ctrl Pts',(178.681581453316,-3.87462682419518,331.967628002819));
#46216=CARTESIAN_POINT('Ctrl Pts',(178.673832568299,-3.95773095032338,332.076928178727));
#46217=CARTESIAN_POINT('Ctrl Pts',(178.666083683282,-4.03608490258727,332.18944814643));
#46218=CARTESIAN_POINT('Ctrl Pts',(178.658326573518,-4.11452202054696,332.302087543991));
#46219=CARTESIAN_POINT('Ctrl Pts',(178.650569463755,-4.18819866928732,332.417953238892));
#46220=CARTESIAN_POINT('Ctrl Pts',(178.642812353991,-4.25685711759007,332.536597770781));
#46221=CARTESIAN_POINT('Ctrl Pts',(178.635051099076,-4.32555225477276,332.655305702515));
#46222=CARTESIAN_POINT('Ctrl Pts',(178.627289844161,-4.3892236669036,332.776795084044));
#46223=CARTESIAN_POINT('Ctrl Pts',(178.619528589246,-4.44766053224136,332.900595595784));
#46224=CARTESIAN_POINT('Ctrl Pts',(178.611754918852,-4.5061908775207,333.024594147999));
#46225=CARTESIAN_POINT('Ctrl Pts',(178.603981248459,-4.55946979114974,333.150910857898));
#46226=CARTESIAN_POINT('Ctrl Pts',(178.596207578065,-4.60733505103374,333.279056424511));
#46227=CARTESIAN_POINT('Ctrl Pts',(178.588795773764,-4.65297217238041,333.40123678638));
#46228=CARTESIAN_POINT('Ctrl Pts',(178.581383969463,-4.69368821862418,333.525079296806));
#46229=CARTESIAN_POINT('Ctrl Pts',(178.573972165163,-4.72938572398217,333.650150476426));
#46230=CARTESIAN_POINT('Ctrl Pts',(178.564222497849,-4.77634308915807,333.814672142449));
#46231=CARTESIAN_POINT('Ctrl Pts',(178.554472830535,-4.8147381632881,333.981738629569));
#46232=CARTESIAN_POINT('Ctrl Pts',(178.544723163222,-4.84434037783941,334.150559380454));
#46233=CARTESIAN_POINT('Ctrl Pts',(178.535124052667,-4.87348546771993,334.316773159823));
#46234=CARTESIAN_POINT('Ctrl Pts',(178.525524942111,-4.894107175471,334.48468753632));
#46235=CARTESIAN_POINT('Ctrl Pts',(178.515925831556,-4.90603092899386,334.653526932857));
#46236=CARTESIAN_POINT('Ctrl Pts',(178.509462637211,-4.91405933286542,334.767208489779));
#46237=CARTESIAN_POINT('Ctrl Pts',(178.502999442865,-4.91814545352143,334.881308968517));
#46238=CARTESIAN_POINT('Ctrl Pts',(178.49653624852,-4.91824801907883,334.995585781249));
#46239=CARTESIAN_POINT('',(181.996536248449,-4.91824818069158,335.004230321965));
#46240=CARTESIAN_POINT('Ctrl Pts',(181.996536248449,-4.91824818069158,335.004230321965));
#46241=CARTESIAN_POINT('Ctrl Pts',(181.987210597247,-4.91810625049596,335.169240912697));
#46242=CARTESIAN_POINT('Ctrl Pts',(181.977884946045,-4.90965625100552,335.333889388984));
#46243=CARTESIAN_POINT('Ctrl Pts',(181.968559294843,-4.8930298995958,335.497434884343));
#46244=CARTESIAN_POINT('Ctrl Pts',(181.959112154449,-4.87618694969273,335.663110955859));
#46245=CARTESIAN_POINT('Ctrl Pts',(181.949665014055,-4.85095328809792,335.827655110689));
#46246=CARTESIAN_POINT('Ctrl Pts',(181.940217873661,-4.81751501808247,335.990319197557));
#46247=CARTESIAN_POINT('Ctrl Pts',(181.931088107924,-4.78520009958176,336.147518619288));
#46248=CARTESIAN_POINT('Ctrl Pts',(181.921958342187,-4.74522291969737,336.302962321272));
#46249=CARTESIAN_POINT('Ctrl Pts',(181.91282857645,-4.69779351779615,336.45599420557));
#46250=CARTESIAN_POINT('Ctrl Pts',(181.905053524964,-4.65740189632902,336.586318554922));
#46251=CARTESIAN_POINT('Ctrl Pts',(181.897278473478,-4.61151922383854,336.715166790492));
#46252=CARTESIAN_POINT('Ctrl Pts',(181.889503421991,-4.56027043970645,336.842041416266));
#46253=CARTESIAN_POINT('Ctrl Pts',(181.881737938622,-4.50908472323853,336.968759907871));
#46254=CARTESIAN_POINT('Ctrl Pts',(181.873972455252,-4.45254617945793,337.093509263252));
#46255=CARTESIAN_POINT('Ctrl Pts',(181.866206971883,-4.39082976365685,337.21580618491));
#46256=CARTESIAN_POINT('Ctrl Pts',(181.858449188395,-4.32917454290447,337.337981842785));
#46257=CARTESIAN_POINT('Ctrl Pts',(181.850691404908,-4.26235184230619,337.457709559476));
#46258=CARTESIAN_POINT('Ctrl Pts',(181.84293362142,-4.19058490167554,337.57452544061));
#46259=CARTESIAN_POINT('Ctrl Pts',(181.835181676256,-4.11887197113864,337.691253408888));
#46260=CARTESIAN_POINT('Ctrl Pts',(181.827429731093,-4.04222241065873,337.805073571734));
#46261=CARTESIAN_POINT('Ctrl Pts',(181.819677785929,-3.96090546396482,337.915546427007));
#46262=CARTESIAN_POINT('Ctrl Pts',(181.811929124124,-3.87962295930347,338.025972491177));
#46263=CARTESIAN_POINT('Ctrl Pts',(181.804180462319,-3.79367723154422,338.133053753465));
#46264=CARTESIAN_POINT('Ctrl Pts',(181.796431800514,-3.70338081158259,338.236379709939));
#46265=CARTESIAN_POINT('Ctrl Pts',(181.788684751125,-3.61310318136283,338.33968416536));
#46266=CARTESIAN_POINT('Ctrl Pts',(181.780937701736,-3.51847691676246,338.439234575164));
#46267=CARTESIAN_POINT('Ctrl Pts',(181.773190652347,-3.41985454242128,338.534653868653));
#46268=CARTESIAN_POINT('Ctrl Pts',(181.765443538239,-3.32123134418514,338.630073959278));
#46269=CARTESIAN_POINT('Ctrl Pts',(181.757696424131,-3.2186122505378,338.721362592959));
#46270=CARTESIAN_POINT('Ctrl Pts',(181.749949310022,-3.11238602376485,338.808180182393));
#46271=CARTESIAN_POINT('Ctrl Pts',(181.742200454374,-3.00613591748659,338.895017288298));
#46272=CARTESIAN_POINT('Ctrl Pts',(181.734451598725,-2.89627736712124,338.977381102642));
#46273=CARTESIAN_POINT('Ctrl Pts',(181.726702743077,-2.78323119818521,339.054973139239));
#46274=CARTESIAN_POINT('Ctrl Pts',(181.718945662805,-2.67006504222195,339.132647531902));
#46275=CARTESIAN_POINT('Ctrl Pts',(181.711188582533,-2.55370483193987,339.205539807943));
#46276=CARTESIAN_POINT('Ctrl Pts',(181.703431502261,-2.43459975534441,339.273395265334));
#46277=CARTESIAN_POINT('Ctrl Pts',(181.695670276952,-2.31543103430932,339.341286981654));
#46278=CARTESIAN_POINT('Ctrl Pts',(181.687909051642,-2.19351487161421,339.404136337351));
#46279=CARTESIAN_POINT('Ctrl Pts',(181.680147826333,-2.06932299717013,339.46173569319));
#46280=CARTESIAN_POINT('Ctrl Pts',(181.672374185441,-1.94493245378691,339.519427190345));
#46281=CARTESIAN_POINT('Ctrl Pts',(181.66460054455,-1.81825928533402,339.571851755619));
#46282=CARTESIAN_POINT('Ctrl Pts',(181.656826903658,-1.68979387444757,339.618850476512));
#46283=CARTESIAN_POINT('Ctrl Pts',(181.649414783164,-1.56730286693722,339.663663478193));
#46284=CARTESIAN_POINT('Ctrl Pts',(181.64200266267,-1.44318284228606,339.703543866795));
#46285=CARTESIAN_POINT('Ctrl Pts',(181.634590542176,-1.31786798642013,339.738397095313));
#46286=CARTESIAN_POINT('Ctrl Pts',(181.626815450207,-1.1864164631764,339.774957086121));
#46287=CARTESIAN_POINT('Ctrl Pts',(181.619040358238,-1.05323471644738,339.806100655392));
#46288=CARTESIAN_POINT('Ctrl Pts',(181.611265266269,-0.918808719549712,
339.83166364717));
#46289=CARTESIAN_POINT('Ctrl Pts',(181.603499741899,-0.784548139855005,
339.857195182542));
#46290=CARTESIAN_POINT('Ctrl Pts',(181.595734217529,-0.649046736773575,
339.877159731758));
#46291=CARTESIAN_POINT('Ctrl Pts',(181.587968693158,-0.512805609667528,
339.891442882135));
#46292=CARTESIAN_POINT('Ctrl Pts',(181.580210868199,-0.376699563770435,
339.905711870965));
#46293=CARTESIAN_POINT('Ctrl Pts',(181.57245304324,-0.239855639646728,339.914310630511));
#46294=CARTESIAN_POINT('Ctrl Pts',(181.56469521828,-0.102784749130356,339.917175851833));
#46295=CARTESIAN_POINT('Ctrl Pts',(181.556943231219,0.0341829931588555,
339.920038917026));
#46296=CARTESIAN_POINT('Ctrl Pts',(181.549191244157,0.171376972665348,339.917177023835));
#46297=CARTESIAN_POINT('Ctrl Pts',(181.541439257096,0.308281894647593,339.908578749081));
#46298=CARTESIAN_POINT('Ctrl Pts',(181.533690552894,0.445128839282379,339.899984115578));
#46299=CARTESIAN_POINT('Ctrl Pts',(181.525941848693,0.581686580569214,339.885657956626));
#46300=CARTESIAN_POINT('Ctrl Pts',(181.518193144491,0.717440784221783,339.865640942737));
#46301=CARTESIAN_POINT('Ctrl Pts',(181.510446052407,0.853166744221293,339.845628093386));
#46302=CARTESIAN_POINT('Ctrl Pts',(181.502698960323,0.988089112662411,339.819926801105));
#46303=CARTESIAN_POINT('Ctrl Pts',(181.494951868238,1.12170002745138,339.788629460599));
#46304=CARTESIAN_POINT('Ctrl Pts',(181.487204711177,1.25531206287902,339.757331857592));
#46305=CARTESIAN_POINT('Ctrl Pts',(181.479457554115,1.38761224214373,339.720438201888));
#46306=CARTESIAN_POINT('Ctrl Pts',(181.471710397053,1.5181046137789,339.678091645546));
#46307=CARTESIAN_POINT('Ctrl Pts',(181.463961498233,1.64862632343256,339.635735568616));
#46308=CARTESIAN_POINT('Ctrl Pts',(181.456212599412,1.77733904496999,339.587924272167));
#46309=CARTESIAN_POINT('Ctrl Pts',(181.448463700592,1.90376403871786,339.534850113001));
#46310=CARTESIAN_POINT('Ctrl Pts',(181.440706577045,2.03032322069275,339.481719620612));
#46311=CARTESIAN_POINT('Ctrl Pts',(181.432949453498,2.15458946333378,339.423315258419));
#46312=CARTESIAN_POINT('Ctrl Pts',(181.425192329951,2.27610549761311,339.359876927877));
#46313=CARTESIAN_POINT('Ctrl Pts',(181.417431061242,2.39768646622964,339.296404697892));
#46314=CARTESIAN_POINT('Ctrl Pts',(181.409669792533,2.51651395967518,339.22789333464));
#46315=CARTESIAN_POINT('Ctrl Pts',(181.401908523823,2.63215808641805,339.15462716385));
#46316=CARTESIAN_POINT('Ctrl Pts',(181.394134839757,2.7479872039459,339.081243792414));
#46317=CARTESIAN_POINT('Ctrl Pts',(181.38636115569,2.86062245755833,339.003090637233));
#46318=CARTESIAN_POINT('Ctrl Pts',(181.378587471623,2.96966483711331,338.920494078265));
#46319=CARTESIAN_POINT('Ctrl Pts',(181.371175817049,3.07362898644098,338.841744136953));
#46320=CARTESIAN_POINT('Ctrl Pts',(181.363764162476,3.17432715178658,338.758955523226));
#46321=CARTESIAN_POINT('Ctrl Pts',(181.356352507902,3.27144492442103,338.672442126022));
#46322=CARTESIAN_POINT('Ctrl Pts',(181.348577429029,3.37332478601966,338.581686616557));
#46323=CARTESIAN_POINT('Ctrl Pts',(181.340802350156,3.47158620445461,338.486545000152));
#46324=CARTESIAN_POINT('Ctrl Pts',(181.333027271284,3.56582814977722,338.387337105863));
#46325=CARTESIAN_POINT('Ctrl Pts',(181.325261760107,3.65995412479419,338.288251292774));
#46326=CARTESIAN_POINT('Ctrl Pts',(181.31749624893,3.7500702015863,338.185109438602));
#46327=CARTESIAN_POINT('Ctrl Pts',(181.309730737753,3.83580899468906,338.07827101126));
#46328=CARTESIAN_POINT('Ctrl Pts',(181.30197292607,3.92146277789733,337.97153851407));
#46329=CARTESIAN_POINT('Ctrl Pts',(181.294215114387,4.00274767133497,337.861117040443));
#46330=CARTESIAN_POINT('Ctrl Pts',(181.286457302703,4.07933395357429,337.747401965078));
#46331=CARTESIAN_POINT('Ctrl Pts',(181.278705328986,4.15586260253463,337.633772463428));
#46332=CARTESIAN_POINT('Ctrl Pts',(181.270953355269,4.22769946073253,337.51685461632));
#46333=CARTESIAN_POINT('Ctrl Pts',(181.263201381552,4.29455606666506,337.397075562591));
#46334=CARTESIAN_POINT('Ctrl Pts',(181.25545269075,4.36138435921617,337.27734723459));
#46335=CARTESIAN_POINT('Ctrl Pts',(181.247703999949,4.42323640425902,337.154760450559));
#46336=CARTESIAN_POINT('Ctrl Pts',(181.239955309147,4.47986806669162,337.029769732639));
#46337=CARTESIAN_POINT('Ctrl Pts',(181.232208230495,4.53648794665621,336.904805019591));
#46338=CARTESIAN_POINT('Ctrl Pts',(181.224461151843,4.58788944317424,336.777437723296));
#46339=CARTESIAN_POINT('Ctrl Pts',(181.21671407319,4.6338754195587,336.648144914293));
#46340=CARTESIAN_POINT('Ctrl Pts',(181.20896692958,4.67986178152939,336.518851021187));
#46341=CARTESIAN_POINT('Ctrl Pts',(181.20121978597,4.72043240181103,336.387631951445));
#46342=CARTESIAN_POINT('Ctrl Pts',(181.193472642359,4.75543927216071,336.25498222748));
#46343=CARTESIAN_POINT('Ctrl Pts',(181.185723756996,4.79045401293386,336.122302680527));
#46344=CARTESIAN_POINT('Ctrl Pts',(181.177974871633,4.8199024149628,335.988192217169));
#46345=CARTESIAN_POINT('Ctrl Pts',(181.170225986271,4.84368716160249,335.853157513609));
#46346=CARTESIAN_POINT('Ctrl Pts',(181.162468876115,4.86749715375857,335.717979482021));
#46347=CARTESIAN_POINT('Ctrl Pts',(181.154711765959,4.88563141408742,335.581875636139));
#46348=CARTESIAN_POINT('Ctrl Pts',(181.146954655804,4.89804422625352,335.445360326213));
#46349=CARTESIAN_POINT('Ctrl Pts',(181.139193400471,4.91046367147038,335.308772066421));
#46350=CARTESIAN_POINT('Ctrl Pts',(181.131432145138,4.9171555573637,335.171772294676));
#46351=CARTESIAN_POINT('Ctrl Pts',(181.123670889806,4.91812634045303,335.034876379429));
#46352=CARTESIAN_POINT('Ctrl Pts',(181.115897218954,4.91909867648387,334.897761474634));
#46353=CARTESIAN_POINT('Ctrl Pts',(181.108123548102,4.91433163504473,334.760751149172));
#46354=CARTESIAN_POINT('Ctrl Pts',(181.100349877251,4.90388374864744,334.624357560636));
#46355=CARTESIAN_POINT('Ctrl Pts',(181.092938076043,4.89392221843911,334.494313186036));
#46356=CARTESIAN_POINT('Ctrl Pts',(181.085526274836,4.87879686579945,334.364829707653));
#46357=CARTESIAN_POINT('Ctrl Pts',(181.078114473628,4.85860150844942,334.236341408355));
#46358=CARTESIAN_POINT('Ctrl Pts',(181.070339398603,4.83741631821718,334.101555525835));
#46359=CARTESIAN_POINT('Ctrl Pts',(181.062564323579,4.81058461613832,333.967438891342));
#46360=CARTESIAN_POINT('Ctrl Pts',(181.054789248554,4.77815833222233,333.834501816941));
#46361=CARTESIAN_POINT('Ctrl Pts',(181.047023741314,4.7457719511656,333.701728331108));
#46362=CARTESIAN_POINT('Ctrl Pts',(181.039258234075,4.70780477825916,333.570131893342));
#46363=CARTESIAN_POINT('Ctrl Pts',(181.031492726836,4.66436028364287,333.440215974285));
#46364=CARTESIAN_POINT('Ctrl Pts',(181.023734919175,4.62095886467914,333.310428868166));
#46365=CARTESIAN_POINT('Ctrl Pts',(181.015977111514,4.57209105480738,333.182319333131));
#46366=CARTESIAN_POINT('Ctrl Pts',(181.008219303853,4.51791090113808,333.056378598626));
#46367=CARTESIAN_POINT('Ctrl Pts',(181.000467334238,4.46377152010305,332.930532639333));
#46368=CARTESIAN_POINT('Ctrl Pts',(180.992715364624,4.40432790642545,332.806852589557));
#46369=CARTESIAN_POINT('Ctrl Pts',(180.984963395009,4.33978314649324,332.68581217186));
#46370=CARTESIAN_POINT('Ctrl Pts',(180.977214708418,4.27526572180386,332.564823015786));
#46371=CARTESIAN_POINT('Ctrl Pts',(180.969466021827,4.20565163123511,332.446471612538));
#46372=CARTESIAN_POINT('Ctrl Pts',(180.961717335236,4.13119097596314,332.331209228392));
#46373=CARTESIAN_POINT('Ctrl Pts',(180.95397026086,4.05674581319582,332.215970826079));
#46374=CARTESIAN_POINT('Ctrl Pts',(180.946223186484,3.97745630345275,332.103820492588));
#46375=CARTESIAN_POINT('Ctrl Pts',(180.938476112108,3.89361694290864,331.995182174508));
#46376=CARTESIAN_POINT('Ctrl Pts',(180.930728972835,3.80977688004724,331.886542946372));
#46377=CARTESIAN_POINT('Ctrl Pts',(180.922981833562,3.72138712916976,331.78141610177));
#46378=CARTESIAN_POINT('Ctrl Pts',(180.915234694289,3.62878344835714,331.680193718388));
#46379=CARTESIAN_POINT('Ctrl Pts',(180.907485813321,3.53615894858904,331.578948578413));
#46380=CARTESIAN_POINT('Ctrl Pts',(180.899736932353,3.43931889752034,331.481609934707));
#46381=CARTESIAN_POINT('Ctrl Pts',(180.891988051386,3.33863670577549,331.388533814453));
#46382=CARTESIAN_POINT('Ctrl Pts',(180.884230945692,3.23784764912627,331.295358902442));
#46383=CARTESIAN_POINT('Ctrl Pts',(180.876473839998,3.13320859292652,331.206455817308));
#46384=CARTESIAN_POINT('Ctrl Pts',(180.868716734305,3.02512732498981,331.122141347328));
#46385=CARTESIAN_POINT('Ctrl Pts',(180.860955483478,2.91698830209655,331.037781822562));
#46386=CARTESIAN_POINT('Ctrl Pts',(180.85319423265,2.80540372011654,330.958016025974));
#46387=CARTESIAN_POINT('Ctrl Pts',(180.845432981823,2.69081045684819,330.883117423606));
#46388=CARTESIAN_POINT('Ctrl Pts',(180.837659315506,2.57603388144784,330.808099007715));
#46389=CARTESIAN_POINT('Ctrl Pts',(180.82988564919,2.45823934315503,330.737963544721));
#46390=CARTESIAN_POINT('Ctrl Pts',(180.822111982873,2.33788920102439,330.672938971284));
#46391=CARTESIAN_POINT('Ctrl Pts',(180.814700135033,2.22314065064444,330.610940909554));
#46392=CARTESIAN_POINT('Ctrl Pts',(180.807288287194,2.10606929737862,330.553588807962));
#46393=CARTESIAN_POINT('Ctrl Pts',(180.799876439354,1.98709111732864,330.501038791684));
#46394=CARTESIAN_POINT('Ctrl Pts',(180.79210135845,1.8622821633874,330.445913452243));
#46395=CARTESIAN_POINT('Ctrl Pts',(180.784326277547,1.73498034195015,330.395898563748));
#46396=CARTESIAN_POINT('Ctrl Pts',(180.776551196643,1.60564288863294,330.351226615904));
#46397=CARTESIAN_POINT('Ctrl Pts',(180.768785683446,1.47646459286564,330.30660963959));
#46398=CARTESIAN_POINT('Ctrl Pts',(180.76102017025,1.34525601531228,330.267322648326));
#46399=CARTESIAN_POINT('Ctrl Pts',(180.753254657053,1.21249652972999,330.233551088295));
#46400=CARTESIAN_POINT('Ctrl Pts',(180.745496843362,1.07986867518179,330.199813012767));
#46401=CARTESIAN_POINT('Ctrl Pts',(180.737739029672,0.945693349134705,330.171579581488));
#46402=CARTESIAN_POINT('Ctrl Pts',(180.729981215982,0.810467001486327,330.148987084948));
#46403=CARTESIAN_POINT('Ctrl Pts',(180.722229240273,0.675342415613457,330.126411589921));
#46404=CARTESIAN_POINT('Ctrl Pts',(180.714477264564,0.539168766413863,330.109468644382));
#46405=CARTESIAN_POINT('Ctrl Pts',(180.706725288855,0.402454319765606,330.098243826647));
#46406=CARTESIAN_POINT('Ctrl Pts',(180.698976596092,0.265797771408406,330.0870237626));
#46407=CARTESIAN_POINT('Ctrl Pts',(180.691227903329,0.128601269872828,330.081517041851));
#46408=CARTESIAN_POINT('Ctrl Pts',(180.683479210566,-0.00862036059448677,
330.081757554585));
#46409=CARTESIAN_POINT('Ctrl Pts',(180.675732129972,-0.145813441167131,
330.081998017278));
#46410=CARTESIAN_POINT('Ctrl Pts',(180.667985049377,-0.283031249644119,
330.087983334336));
#46411=CARTESIAN_POINT('Ctrl Pts',(180.660237968783,-0.419757910862382,
330.099695278988));
#46412=CARTESIAN_POINT('Ctrl Pts',(180.652490823251,-0.556485718147188,
330.111407321812));
#46413=CARTESIAN_POINT('Ctrl Pts',(180.644743677719,-0.692721980513987,
330.128846054614));
#46414=CARTESIAN_POINT('Ctrl Pts',(180.636996532187,-0.82795529290341,330.151941306517));
#46415=CARTESIAN_POINT('Ctrl Pts',(180.629247644925,-0.963219008731504,
330.175041750744));
#46416=CARTESIAN_POINT('Ctrl Pts',(180.621498757664,-1.09747894067125,330.203801178847));
#46417=CARTESIAN_POINT('Ctrl Pts',(180.613749870402,-1.23023362338467,330.238098248137));
#46418=CARTESIAN_POINT('Ctrl Pts',(180.605992758395,-1.36312921323199,330.272431720676));
#46419=CARTESIAN_POINT('Ctrl Pts',(180.598235646388,-1.49451598327833,330.312314477747));
#46420=CARTESIAN_POINT('Ctrl Pts',(180.59047853438,-1.6239068615804,330.357575033734));
#46421=CARTESIAN_POINT('Ctrl Pts',(180.582717277219,-1.75336688226033,330.402859775525));
#46422=CARTESIAN_POINT('Ctrl Pts',(180.574956020057,-1.88082852297318,330.453527898072));
#46423=CARTESIAN_POINT('Ctrl Pts',(180.567194762895,-2.00582540012955,330.509360009231));
#46424=CARTESIAN_POINT('Ctrl Pts',(180.559421090273,-2.13102223121361,330.56528143342));
#46425=CARTESIAN_POINT('Ctrl Pts',(180.55164741765,-2.25374606974708,330.626383179212));
#46426=CARTESIAN_POINT('Ctrl Pts',(180.543873745028,-2.37355502941302,330.692399788183));
#46427=CARTESIAN_POINT('Ctrl Pts',(180.536461965045,-2.48778644770066,330.755343084696));
#46428=CARTESIAN_POINT('Ctrl Pts',(180.529050185062,-2.59936802770936,330.822753787484));
#46429=CARTESIAN_POINT('Ctrl Pts',(180.52163840508,-2.70794338199464,330.894366589379));
#46430=CARTESIAN_POINT('Ctrl Pts',(180.513878670321,-2.82161593468427,330.969341338944));
#46431=CARTESIAN_POINT('Ctrl Pts',(180.506118935562,-2.93235554456295,331.049161358738));
#46432=CARTESIAN_POINT('Ctrl Pts',(180.498359200804,-3.03972028326498,331.133569648628));
#46433=CARTESIAN_POINT('Ctrl Pts',(180.490609025355,-3.14695275805946,331.217873954936));
#46434=CARTESIAN_POINT('Ctrl Pts',(180.482858849906,-3.25081832769985,331.306755045375));
#46435=CARTESIAN_POINT('Ctrl Pts',(180.475108674458,-3.35090255687002,331.399911790405));
#46436=CARTESIAN_POINT('Ctrl Pts',(180.467366173794,-3.4508876753905,331.492976284883));
#46437=CARTESIAN_POINT('Ctrl Pts',(180.45962367313,-3.54709861924634,331.590307742795));
#46438=CARTESIAN_POINT('Ctrl Pts',(180.451881172467,-3.63915298617011,331.691564024233));
#46439=CARTESIAN_POINT('Ctrl Pts',(180.444144468867,-3.73113842897115,331.792744491773));
#46440=CARTESIAN_POINT('Ctrl Pts',(180.436407765267,-3.81897322598363,331.897843644671));
#46441=CARTESIAN_POINT('Ctrl Pts',(180.428671061668,-3.90231118561838,332.006481923706));
#46442=CARTESIAN_POINT('Ctrl Pts',(180.420937575272,-3.98561449028321,332.115075026974));
#46443=CARTESIAN_POINT('Ctrl Pts',(180.413204088877,-4.06442443789406,332.227204018703));
#46444=CARTESIAN_POINT('Ctrl Pts',(180.405470602481,-4.13843473160768,332.342455826383));
#46445=CARTESIAN_POINT('Ctrl Pts',(180.397738661595,-4.21243023462844,332.457684601402));
#46446=CARTESIAN_POINT('Ctrl Pts',(180.39000672071,-4.281627779502,332.576034620936));
#46447=CARTESIAN_POINT('Ctrl Pts',(180.382274779824,-4.34576432241902,332.697063718535));
#46448=CARTESIAN_POINT('Ctrl Pts',(180.374542692827,-4.4099020773275,332.818095103226));
#46449=CARTESIAN_POINT('Ctrl Pts',(180.36681060583,-4.46897845602357,332.941805319855));
#46450=CARTESIAN_POINT('Ctrl Pts',(180.359078518834,-4.52277652114452,333.067727865366));
#46451=CARTESIAN_POINT('Ctrl Pts',(180.351344594356,-4.57658737102809,333.193680335556));
#46452=CARTESIAN_POINT('Ctrl Pts',(180.343610669879,-4.62511725738823,333.321845819719));
#46453=CARTESIAN_POINT('Ctrl Pts',(180.335876745402,-4.6681976659552,333.451738518831));
#46454=CARTESIAN_POINT('Ctrl Pts',(180.328134605733,-4.71132383574079,333.581769193613));
#46455=CARTESIAN_POINT('Ctrl Pts',(180.320392466064,-4.74898884220444,333.713530374675));
#46456=CARTESIAN_POINT('Ctrl Pts',(180.312650326396,-4.78107414634263,333.846521318067));
#46457=CARTESIAN_POINT('Ctrl Pts',(180.304903927326,-4.81317710246988,333.9795854275));
#46458=CARTESIAN_POINT('Ctrl Pts',(180.297157528257,-4.83969416457988,334.113880262331));
#46459=CARTESIAN_POINT('Ctrl Pts',(180.289411129187,-4.8605582812456,334.248896640192));
#46460=CARTESIAN_POINT('Ctrl Pts',(180.281652613415,-4.88145503298411,334.384124206928));
#46461=CARTESIAN_POINT('Ctrl Pts',(180.273894097643,-4.89668112984652,334.520075181497));
#46462=CARTESIAN_POINT('Ctrl Pts',(180.266135581871,-4.90622151443417,334.656236252925));
#46463=CARTESIAN_POINT('Ctrl Pts',(180.259602470754,-4.91425506033938,334.770891611707));
#46464=CARTESIAN_POINT('Ctrl Pts',(180.253069359637,-4.91825801731504,334.885695792017));
#46465=CARTESIAN_POINT('Ctrl Pts',(180.24653624852,-4.91824998793836,335.000344447839));
#46466=CARTESIAN_POINT('',(183.746536248537,-4.91824946343417,334.997702625515));
#46467=CARTESIAN_POINT('Ctrl Pts',(183.74653624849,-4.91824946343456,334.997702626357));
#46468=CARTESIAN_POINT('Ctrl Pts',(183.738662233524,-4.91831472035729,335.137405554579));
#46469=CARTESIAN_POINT('Ctrl Pts',(183.730788218558,-4.91242323172791,335.277092861909));
#46470=CARTESIAN_POINT('Ctrl Pts',(183.722914203592,-4.9006054591028,335.416232142814));
#46471=CARTESIAN_POINT('Ctrl Pts',(183.715037492967,-4.88878364067781,335.555419057881));
#46472=CARTESIAN_POINT('Ctrl Pts',(183.707160782342,-4.87103152767783,335.694057201196));
#46473=CARTESIAN_POINT('Ctrl Pts',(183.699284071717,-4.8474314120948,335.831619965812));
#46474=CARTESIAN_POINT('Ctrl Pts',(183.691403188189,-4.82381879370446,335.969255608067));
#46475=CARTESIAN_POINT('Ctrl Pts',(183.68352230466,-4.79435206354287,336.10581436943));
#46476=CARTESIAN_POINT('Ctrl Pts',(183.675641421132,-4.75916446642854,336.240780659095));
#46477=CARTESIAN_POINT('Ctrl Pts',(183.667749095471,-4.72392578098497,336.375942904233));
#46478=CARTESIAN_POINT('Ctrl Pts',(183.659856769809,-4.68294972730786,336.509507696768));
#46479=CARTESIAN_POINT('Ctrl Pts',(183.651964444148,-4.63641950913448,336.640974465925));
#46480=CARTESIAN_POINT('Ctrl Pts',(183.644066234623,-4.58985460188793,336.772539245805));
#46481=CARTESIAN_POINT('Ctrl Pts',(183.636168025098,-4.53772741418317,336.902002538605));
#46482=CARTESIAN_POINT('Ctrl Pts',(183.628269815572,-4.48026877631966,337.028885101339));
#46483=CARTESIAN_POINT('Ctrl Pts',(183.620356925575,-4.42270333957709,337.156003501815));
#46484=CARTESIAN_POINT('Ctrl Pts',(183.612444035578,-4.35978681345751,337.280531251256));
#46485=CARTESIAN_POINT('Ctrl Pts',(183.604531145581,-4.29179594580606,337.402013868));
#46486=CARTESIAN_POINT('Ctrl Pts',(183.597106357752,-4.22799905657679,337.51600289787));
#46487=CARTESIAN_POINT('Ctrl Pts',(183.589681569923,-4.15973509277527,337.627310935476));
#46488=CARTESIAN_POINT('Ctrl Pts',(183.582256782094,-4.08726574767666,337.735588011812));
#46489=CARTESIAN_POINT('Ctrl Pts',(183.574483044214,-4.01139048954663,337.848953892314));
#46490=CARTESIAN_POINT('Ctrl Pts',(183.566709306335,-3.93067481074444,337.959340381255));
#46491=CARTESIAN_POINT('Ctrl Pts',(183.558935568455,-3.84538014502149,338.066306345226));
#46492=CARTESIAN_POINT('Ctrl Pts',(183.55117141566,-3.76019064834008,338.173140419262));
#46493=CARTESIAN_POINT('Ctrl Pts',(183.543407262865,-3.67043363986846,338.27656205715));
#46494=CARTESIAN_POINT('Ctrl Pts',(183.535643110069,-3.5764144512764,338.376157984337));
#46495=CARTESIAN_POINT('Ctrl Pts',(183.527886672613,-3.48248869076345,338.475654941767));
#46496=CARTESIAN_POINT('Ctrl Pts',(183.520130235156,-3.38430944539702,338.571333471441));
#46497=CARTESIAN_POINT('Ctrl Pts',(183.5123737977,-3.28222280124049,338.662812654985));
#46498=CARTESIAN_POINT('Ctrl Pts',(183.504623212537,-3.18021318227063,338.754222816756));
#46499=CARTESIAN_POINT('Ctrl Pts',(183.496872627374,-3.0743023226734,338.841439679069));
#46500=CARTESIAN_POINT('Ctrl Pts',(183.489122042212,-2.96487345396073,338.924118813759));
#46501=CARTESIAN_POINT('Ctrl Pts',(183.481374756881,-2.8554911748783,339.006762747589));
#46502=CARTESIAN_POINT('Ctrl Pts',(183.473627471551,-2.7425941770438,339.084872561081));
#46503=CARTESIAN_POINT('Ctrl Pts',(183.46588018622,-2.62659891860498,339.158143958942));
#46504=CARTESIAN_POINT('Ctrl Pts',(183.458134523145,-2.51062794918574,339.231400014017));
#46505=CARTESIAN_POINT('Ctrl Pts',(183.45038886007,-2.39156033998065,339.299819459971));
#46506=CARTESIAN_POINT('Ctrl Pts',(183.442643196996,-2.26984135408545,339.363141447373));
#46507=CARTESIAN_POINT('Ctrl Pts',(183.43489747775,-2.14812148550022,339.426463893977));
#46508=CARTESIAN_POINT('Ctrl Pts',(183.427151758505,-2.02375054875627,339.484688627805));
#46509=CARTESIAN_POINT('Ctrl Pts',(183.419406039259,-1.89719785537914,339.537601057833));
#46510=CARTESIAN_POINT('Ctrl Pts',(183.411658585736,-1.77061682666147,339.590525335034));
#46511=CARTESIAN_POINT('Ctrl Pts',(183.403911132212,-1.64185342995883,339.638134790811));
#46512=CARTESIAN_POINT('Ctrl Pts',(183.396163678688,-1.51139599080171,339.680263370953));
#46513=CARTESIAN_POINT('Ctrl Pts',(183.388408004165,-1.38080012027327,339.722436654696));
#46514=CARTESIAN_POINT('Ctrl Pts',(183.380652329641,-1.24850698914037,339.759117324682));
#46515=CARTESIAN_POINT('Ctrl Pts',(183.372896655117,-1.11501962321825,339.790189380634));
#46516=CARTESIAN_POINT('Ctrl Pts',(183.365136839753,-0.981460986919521,
339.821278026299));
#46517=CARTESIAN_POINT('Ctrl Pts',(183.357377024389,-0.846707229366385,
339.846752018567));
#46518=CARTESIAN_POINT('Ctrl Pts',(183.349617209025,-0.711269560545343,
339.866546894333));
#46519=CARTESIAN_POINT('Ctrl Pts',(183.34184497105,-0.57561507091135,339.886373459518));
#46520=CARTESIAN_POINT('Ctrl Pts',(183.334072733075,-0.439274871295413,
339.900502700093));
#46521=CARTESIAN_POINT('Ctrl Pts',(183.326300495101,-0.302764153413162,
339.908922175988));
#46522=CARTESIAN_POINT('Ctrl Pts',(183.318873246007,-0.172312781626706,
339.91696793384));
#46523=CARTESIAN_POINT('Ctrl Pts',(183.311445996913,-0.0417059970710242,
339.919799946453));
#46524=CARTESIAN_POINT('Ctrl Pts',(183.304018747819,0.0886102589325586,
339.917451706373));
#46525=CARTESIAN_POINT('Ctrl Pts',(183.296243208508,0.225037509280272,339.914993348935));
#46526=CARTESIAN_POINT('Ctrl Pts',(183.288467669196,0.361577749274374,339.906849358024));
#46527=CARTESIAN_POINT('Ctrl Pts',(183.280692129884,0.497718315349884,339.893001077158));
#46528=CARTESIAN_POINT('Ctrl Pts',(183.272926154675,0.6336914252225,339.879169830013));
#46529=CARTESIAN_POINT('Ctrl Pts',(183.265160179465,0.769265454236493,339.859648292778));
#46530=CARTESIAN_POINT('Ctrl Pts',(183.257394204256,0.903927437011325,339.834469800414));
#46531=CARTESIAN_POINT('Ctrl Pts',(183.249635925466,1.03845596389929,339.809316261033));
#46532=CARTESIAN_POINT('Ctrl Pts',(183.241877646676,1.17207386162816,339.778516994751));
#46533=CARTESIAN_POINT('Ctrl Pts',(183.234119367886,1.30427334318214,339.742157115571));
#46534=CARTESIAN_POINT('Ctrl Pts',(183.226366924501,1.43637339062766,339.705824584549));
#46535=CARTESIAN_POINT('Ctrl Pts',(183.218614481116,1.56705677013313,339.66393986879));
#46536=CARTESIAN_POINT('Ctrl Pts',(183.210862037731,1.69582629933627,339.616639061588));
#46537=CARTESIAN_POINT('Ctrl Pts',(183.203112875046,1.82454133550684,339.569358271267));
#46538=CARTESIAN_POINT('Ctrl Pts',(183.195363712361,1.95134376613767,339.516666082607));
#46539=CARTESIAN_POINT('Ctrl Pts',(183.187614549676,2.07575219336666,339.458748242975));
#46540=CARTESIAN_POINT('Ctrl Pts',(183.179866997861,2.20013475898928,339.40084244311));
#46541=CARTESIAN_POINT('Ctrl Pts',(183.172119446045,2.32212395700371,339.337713317832));
#46542=CARTESIAN_POINT('Ctrl Pts',(183.16437189423,2.44125935066559,339.269594342006));
#46543=CARTESIAN_POINT('Ctrl Pts',(183.156624276629,2.5603957559335,339.201474787765));
#46544=CARTESIAN_POINT('Ctrl Pts',(183.148876659027,2.67667796924099,339.12836549246));
#46545=CARTESIAN_POINT('Ctrl Pts',(183.141129041426,2.78967145085819,339.050545180438));
#46546=CARTESIAN_POINT('Ctrl Pts',(183.133379681695,2.90269034018911,338.972707369741));
#46547=CARTESIAN_POINT('Ctrl Pts',(183.125630321964,3.01241870448798,338.890156656029));
#46548=CARTESIAN_POINT('Ctrl Pts',(183.117880962233,3.11845253832436,338.803214013005));
#46549=CARTESIAN_POINT('Ctrl Pts',(183.110123379805,3.22459888263836,338.716179116802));
#46550=CARTESIAN_POINT('Ctrl Pts',(183.102365797376,3.32704256283489,338.624743230307));
#46551=CARTESIAN_POINT('Ctrl Pts',(183.094608214948,3.42541371574121,338.529266770664));
#46552=CARTESIAN_POINT('Ctrl Pts',(183.086846487737,3.52383742716301,338.433739299105));
#46553=CARTESIAN_POINT('Ctrl Pts',(183.079084760526,3.61818400692725,338.334167236275));
#46554=CARTESIAN_POINT('Ctrl Pts',(183.071323033316,3.70812250454873,338.230945767691));
#46555=CARTESIAN_POINT('Ctrl Pts',(183.063548896042,3.79820480294702,338.127559260467));
#46556=CARTESIAN_POINT('Ctrl Pts',(183.055774758768,3.88386469091444,338.02051199282));
#46557=CARTESIAN_POINT('Ctrl Pts',(183.048000621495,3.96481281290701,337.910230647407));
#46558=CARTESIAN_POINT('Ctrl Pts',(183.040593985512,4.04193433160511,337.805162554005));
#46559=CARTESIAN_POINT('Ctrl Pts',(183.033187349529,4.11477920662459,337.697159390882));
#46560=CARTESIAN_POINT('Ctrl Pts',(183.025780713546,4.18313606116424,337.586610862942));
#46561=CARTESIAN_POINT('Ctrl Pts',(183.018005522485,4.25489436082336,337.470561427252));
#46562=CARTESIAN_POINT('Ctrl Pts',(183.010230331425,4.32193314534969,337.351340323045));
#46563=CARTESIAN_POINT('Ctrl Pts',(183.002455140365,4.38395929370328,337.229368514547));
#46564=CARTESIAN_POINT('Ctrl Pts',(182.994689514232,4.44590913838514,337.107546754006));
#46565=CARTESIAN_POINT('Ctrl Pts',(182.986923888099,4.50285844093783,336.982981367197));
#46566=CARTESIAN_POINT('Ctrl Pts',(182.979158261967,4.55455763588336,336.856121710426));
#46567=CARTESIAN_POINT('Ctrl Pts',(182.971400332695,4.6062055894306,336.72938778997));
#46568=CARTESIAN_POINT('Ctrl Pts',(182.963642403424,4.6526136443135,336.600364484482));
#46569=CARTESIAN_POINT('Ctrl Pts',(182.955884474153,4.69357857819171,336.469524818722));
#46570=CARTESIAN_POINT('Ctrl Pts',(182.948132380349,4.73451269849694,336.338783569759));
#46571=CARTESIAN_POINT('Ctrl Pts',(182.940380286544,4.77001173095744,336.206229051496));
#46572=CARTESIAN_POINT('Ctrl Pts',(182.93262819274,4.79992106078274,336.072352960902));
#46573=CARTESIAN_POINT('Ctrl Pts',(182.924879378459,4.82981773746841,335.938533506577));
#46574=CARTESIAN_POINT('Ctrl Pts',(182.917130564177,4.85412932973476,335.803393972577));
#46575=CARTESIAN_POINT('Ctrl Pts',(182.909381749896,4.87275151938588,335.667439654817));
#46576=CARTESIAN_POINT('Ctrl Pts',(182.901634545713,4.89136983959658,335.531513586535));
#46577=CARTESIAN_POINT('Ctrl Pts',(182.893887341531,4.90430105562567,335.394773458246));
#46578=CARTESIAN_POINT('Ctrl Pts',(182.886140137349,4.911492327446,335.257732768462));
#46579=CARTESIAN_POINT('Ctrl Pts',(182.878392866271,4.91868366136183,335.120690895353));
#46580=CARTESIAN_POINT('Ctrl Pts',(182.870645595193,4.92013493173456,334.983348845895));
#46581=CARTESIAN_POINT('Ctrl Pts',(182.862898324115,4.91584536414341,334.846222828971));
#46582=CARTESIAN_POINT('Ctrl Pts',(182.855149309458,4.9115548311543,334.709065950853));
#46583=CARTESIAN_POINT('Ctrl Pts',(182.847400294801,4.90152090144786,334.572125592609));
#46584=CARTESIAN_POINT('Ctrl Pts',(182.839651280144,4.88579485286582,334.435915149814));
#46585=CARTESIAN_POINT('Ctrl Pts',(182.831894038515,4.8700521082577,334.29956009516));
#46586=CARTESIAN_POINT('Ctrl Pts',(182.824136796887,4.84860521780202,334.163936892858));
#46587=CARTESIAN_POINT('Ctrl Pts',(182.816379555258,4.82155710453961,334.029551572641));
#46588=CARTESIAN_POINT('Ctrl Pts',(182.808618167059,4.79449453292637,333.895094417835));
#46589=CARTESIAN_POINT('Ctrl Pts',(182.80085677886,4.76182486556082,333.76187684303));
#46590=CARTESIAN_POINT('Ctrl Pts',(182.79309539066,4.7237013206043,333.630390969575));
#46591=CARTESIAN_POINT('Ctrl Pts',(182.785321585883,4.68551678604702,333.49869474656));
#46592=CARTESIAN_POINT('Ctrl Pts',(182.777547781106,4.64186106319591,333.368736131593));
#46593=CARTESIAN_POINT('Ctrl Pts',(182.769773976329,4.5929363660258,333.240989312102));
#46594=CARTESIAN_POINT('Ctrl Pts',(182.762363543976,4.5462985652168,333.119213786325));
#46595=CARTESIAN_POINT('Ctrl Pts',(182.754953111624,4.49487334525659,332.99944822182));
#46596=CARTESIAN_POINT('Ctrl Pts',(182.747542679272,4.43887438890023,332.882081866061));
#46597=CARTESIAN_POINT('Ctrl Pts',(182.739767793996,4.38012134446927,332.75894330843));
#46598=CARTESIAN_POINT('Ctrl Pts',(182.73199290872,4.31614755979411,332.638056719292));
#46599=CARTESIAN_POINT('Ctrl Pts',(182.724218023444,4.24714834915519,332.519896380639));
#46600=CARTESIAN_POINT('Ctrl Pts',(182.716452708519,4.17823407181412,332.401881489262));
#46601=CARTESIAN_POINT('Ctrl Pts',(182.708687393594,4.1043068720002,332.286586505573));
#46602=CARTESIAN_POINT('Ctrl Pts',(182.700922078669,4.02560951209295,332.174464454542));
#46603=CARTESIAN_POINT('Ctrl Pts',(182.693164465668,3.94699020711559,332.062453610276));
#46604=CARTESIAN_POINT('Ctrl Pts',(182.685406852667,3.86361038055084,331.953609753793));
#46605=CARTESIAN_POINT('Ctrl Pts',(182.677649239666,3.77575777952021,331.848359751987));
#46606=CARTESIAN_POINT('Ctrl Pts',(182.669897466842,3.68797131671046,331.743188985718));
#46607=CARTESIAN_POINT('Ctrl Pts',(182.662145694018,3.59571903124513,331.641606987716));
#46608=CARTESIAN_POINT('Ctrl Pts',(182.654393921194,3.49933067914566,331.544009858161));
#46609=CARTESIAN_POINT('Ctrl Pts',(182.646645433943,3.40298318104794,331.446454094945));
#46610=CARTESIAN_POINT('Ctrl Pts',(182.638896946692,3.3025033771423,331.35288011846));
#46611=CARTESIAN_POINT('Ctrl Pts',(182.63114845944,3.19825967999946,331.263649095469));
#46612=CARTESIAN_POINT('Ctrl Pts',(182.623401585928,3.09403769317387,331.17443665618));
#46613=CARTESIAN_POINT('Ctrl Pts',(182.615654712416,2.98605366909098,331.089565625335));
#46614=CARTESIAN_POINT('Ctrl Pts',(182.607907838903,2.87471077863055,331.009358322058));
#46615=CARTESIAN_POINT('Ctrl Pts',(182.600160901831,2.76336697465094,330.929150360716));
#46616=CARTESIAN_POINT('Ctrl Pts',(182.592413964759,2.64866456649613,330.853606431745));
#46617=CARTESIAN_POINT('Ctrl Pts',(182.584667027687,2.53103718259929,330.783006539868));
#46618=CARTESIAN_POINT('Ctrl Pts',(182.576918350071,2.41338337075461,330.71239078595));
#46619=CARTESIAN_POINT('Ctrl Pts',(182.569169672455,2.29280361057261,330.646721480619));
#46620=CARTESIAN_POINT('Ctrl Pts',(182.561420994839,2.16975733561803,330.586233335683));
#46621=CARTESIAN_POINT('Ctrl Pts',(182.553664093177,2.04658046570813,330.525680991758));
#46622=CARTESIAN_POINT('Ctrl Pts',(182.545907191515,1.92093220301761,330.470320965749));
#46623=CARTESIAN_POINT('Ctrl Pts',(182.538150289853,1.79329373726262,330.420340554758));
#46624=CARTESIAN_POINT('Ctrl Pts',(182.53038924375,1.66558707545349,330.370333439695));
#46625=CARTESIAN_POINT('Ctrl Pts',(182.522628197647,1.53588846121267,330.325711794006));
#46626=CARTESIAN_POINT('Ctrl Pts',(182.514867151544,1.40469460780011,330.28661309446));
#46627=CARTESIAN_POINT('Ctrl Pts',(182.507093689075,1.27329086632136,330.24745184358));
#46628=CARTESIAN_POINT('Ctrl Pts',(182.499320226606,1.14038748464425,330.21383129127));
#46629=CARTESIAN_POINT('Ctrl Pts',(182.491546764136,1.00649261114424,330.185838007897));
#46630=CARTESIAN_POINT('Ctrl Pts',(182.484132724423,0.878788655103757,330.159139054189));
#46631=CARTESIAN_POINT('Ctrl Pts',(182.476718684711,0.750183129836309,330.137558670627));
#46632=CARTESIAN_POINT('Ctrl Pts',(182.469304644998,0.62111967389052,330.12112785439));
#46633=CARTESIAN_POINT('Ctrl Pts',(182.461529486789,0.485769874346384,330.103896736041));
#46634=CARTESIAN_POINT('Ctrl Pts',(182.45375432858,0.349488651101491,330.092274978123));
#46635=CARTESIAN_POINT('Ctrl Pts',(182.445979170372,0.212780573065129,330.086354969045));
#46636=CARTESIAN_POINT('Ctrl Pts',(182.438213579175,0.0762407086890431,
330.080442244295));
#46637=CARTESIAN_POINT('Ctrl Pts',(182.430447987978,-0.0607245786593256,
330.080217325762));
#46638=CARTESIAN_POINT('Ctrl Pts',(182.422682396782,-0.197602922753006,
330.08572119763));
#46639=CARTESIAN_POINT('Ctrl Pts',(182.414924504484,-0.334345564028642,
330.091219612895));
#46640=CARTESIAN_POINT('Ctrl Pts',(182.407166612187,-0.471001045551423,
330.102435500246));
#46641=CARTESIAN_POINT('Ctrl Pts',(182.39940871989,-0.607054657868781,330.119357859373));
#46642=CARTESIAN_POINT('Ctrl Pts',(182.391656665053,-0.743005896038143,
330.136267485196));
#46643=CARTESIAN_POINT('Ctrl Pts',(182.383904610217,-0.878355780121441,
330.158874988023));
#46644=CARTESIAN_POINT('Ctrl Pts',(182.37615255538,-1.01259274292381,330.187117391887));
#46645=CARTESIAN_POINT('Ctrl Pts',(182.368403782979,-1.14677286605946,330.21534783713));
#46646=CARTESIAN_POINT('Ctrl Pts',(182.360655010579,-1.27984062348581,330.249208357569));
#46647=CARTESIAN_POINT('Ctrl Pts',(182.352906238178,-1.41129290768061,330.288584566053));
#46648=CARTESIAN_POINT('Ctrl Pts',(182.345159077646,-1.54271784768671,330.327952583653));
#46649=CARTESIAN_POINT('Ctrl Pts',(182.337411917115,-1.67252760868526,330.372833895044));
#46650=CARTESIAN_POINT('Ctrl Pts',(182.329664756583,-1.80023294365699,330.423063862028));
#46651=CARTESIAN_POINT('Ctrl Pts',(182.321917530891,-1.92793935274515,330.473294251491));
#46652=CARTESIAN_POINT('Ctrl Pts',(182.314170305199,-2.05354093676256,330.528873243206));
#46653=CARTESIAN_POINT('Ctrl Pts',(182.306423079507,-2.17656755136495,330.589587688566));
#46654=CARTESIAN_POINT('Ctrl Pts',(182.298674111938,-2.2996218271253,330.65031578489));
#46655=CARTESIAN_POINT('Ctrl Pts',(182.290925144369,-2.42009963098066,330.71618145954));
#46656=CARTESIAN_POINT('Ctrl Pts',(182.2831761768,-2.53755494317087,330.786925353986));
#46657=CARTESIAN_POINT('Ctrl Pts',(182.275418984706,-2.65513491894708,330.857744333904));
#46658=CARTESIAN_POINT('Ctrl Pts',(182.267661792613,-2.76968565945884,330.933451674372));
#46659=CARTESIAN_POINT('Ctrl Pts',(182.259904600519,-2.88078924456396,331.013744063547));
#46660=CARTESIAN_POINT('Ctrl Pts',(182.252143263265,-2.99195219937276,331.094079358047));
#46661=CARTESIAN_POINT('Ctrl Pts',(182.244381926011,-3.09966402157302,331.179004341388));
#46662=CARTESIAN_POINT('Ctrl Pts',(182.236620588757,-3.20354028590892,331.268175687541));
#46663=CARTESIAN_POINT('Ctrl Pts',(182.228846836842,-3.30758270571109,331.357489667882));
#46664=CARTESIAN_POINT('Ctrl Pts',(182.221073084927,-3.40777702194416,331.451063317094));
#46665=CARTESIAN_POINT('Ctrl Pts',(182.213299333012,-3.50377542993101,331.548516145321));
#46666=CARTESIAN_POINT('Ctrl Pts',(182.205888425583,-3.59529305523456,331.641420304936));
#46667=CARTESIAN_POINT('Ctrl Pts',(182.198477518153,-3.6829974302838,331.737849479016));
#46668=CARTESIAN_POINT('Ctrl Pts',(182.191066610724,-3.76662275388509,331.837447851432));
#46669=CARTESIAN_POINT('Ctrl Pts',(182.182961178964,-3.85808515039839,331.946380235041));
#46670=CARTESIAN_POINT('Ctrl Pts',(182.174855747204,-3.94498091133261,332.059477675757));
#46671=CARTESIAN_POINT('Ctrl Pts',(182.166750315444,-4.0269075543671,332.176314711041));
#46672=CARTESIAN_POINT('Ctrl Pts',(182.159031256342,-4.10492888850736,332.28758231621));
#46673=CARTESIAN_POINT('Ctrl Pts',(182.151312197239,-4.17844356562488,332.402240893272));
#46674=CARTESIAN_POINT('Ctrl Pts',(182.143593138136,-4.24714239787314,332.519886189166));
#46675=CARTESIAN_POINT('Ctrl Pts',(182.135881261439,-4.31577730744665,332.637422018833));
#46676=CARTESIAN_POINT('Ctrl Pts',(182.128169384742,-4.37960508622303,332.757938700952));
#46677=CARTESIAN_POINT('Ctrl Pts',(182.120457508046,-4.4383588660141,332.881001736911));
#46678=CARTESIAN_POINT('Ctrl Pts',(182.112751089534,-4.49707106202213,333.00397767334));
#46679=CARTESIAN_POINT('Ctrl Pts',(182.105044671022,-4.55071623349502,333.129496022812));
#46680=CARTESIAN_POINT('Ctrl Pts',(182.097338252511,-4.59907286804657,333.257096727613));
#46681=CARTESIAN_POINT('Ctrl Pts',(182.089635572285,-4.6474060454057,333.384635534924));
#46682=CARTESIAN_POINT('Ctrl Pts',(182.08193289206,-4.69045565138616,333.514254318132));
#46683=CARTESIAN_POINT('Ctrl Pts',(182.074230211834,-4.72804803173018,333.645472454266));
#46684=CARTESIAN_POINT('Ctrl Pts',(182.066528352036,-4.76563640803903,333.776676614109));
#46685=CARTESIAN_POINT('Ctrl Pts',(182.058826492237,-4.79776859951033,333.909479409798));
#46686=CARTESIAN_POINT('Ctrl Pts',(182.051124632439,-4.8243206934159,334.043384659553));
#46687=CARTESIAN_POINT('Ctrl Pts',(182.04342322529,-4.85087122681638,334.177282039502));
#46688=CARTESIAN_POINT('Ctrl Pts',(182.035721818141,-4.87184224376834,334.312281355446));
#46689=CARTESIAN_POINT('Ctrl Pts',(182.028020410992,-4.88716101142139,334.447876543749));
#46690=CARTESIAN_POINT('Ctrl Pts',(182.020315803866,-4.90248614410664,334.583528072599));
#46691=CARTESIAN_POINT('Ctrl Pts',(182.01261119674,-4.91215429899052,334.719775574408));
#46692=CARTESIAN_POINT('Ctrl Pts',(182.004906589614,-4.91614465092684,334.85610825714));
#46693=CARTESIAN_POINT('Ctrl Pts',(182.002116475906,-4.91758970003254,334.905479195944));
#46694=CARTESIAN_POINT('Ctrl Pts',(181.999326362198,-4.91829064435592,334.954861295829));
#46695=CARTESIAN_POINT('Ctrl Pts',(181.99653624849,-4.91824818069221,335.00423032124));
#46696=CARTESIAN_POINT('',(185.231450264354,-2.85698122534213,339.003353761603));
#46697=CARTESIAN_POINT('Ctrl Pts',(185.231450264354,-2.85698122534213,339.003353761603));
#46698=CARTESIAN_POINT('Ctrl Pts',(185.223817702065,-2.74793304536805,339.081175663288));
#46699=CARTESIAN_POINT('Ctrl Pts',(185.216185139776,-2.63549753799294,339.154684880481));
#46700=CARTESIAN_POINT('Ctrl Pts',(185.208552577486,-2.52005774144929,339.223563902945));
#46701=CARTESIAN_POINT('Ctrl Pts',(185.200929512,-2.40476158067637,339.292357222803));
#46702=CARTESIAN_POINT('Ctrl Pts',(185.193306446513,-2.28646890749794,339.356531596598));
#46703=CARTESIAN_POINT('Ctrl Pts',(185.185683381027,-2.16559473885085,339.415810513322));
#46704=CARTESIAN_POINT('Ctrl Pts',(185.178067826808,-2.04483967167305,339.475031020493));
#46705=CARTESIAN_POINT('Ctrl Pts',(185.17045227259,-1.92150852917018,339.529365485536));
#46706=CARTESIAN_POINT('Ctrl Pts',(185.162836718371,-1.79604366280304,339.578581682552));
#46707=CARTESIAN_POINT('Ctrl Pts',(185.154945478167,-1.66603692011077,339.629579524793));
#46708=CARTESIAN_POINT('Ctrl Pts',(185.147054237962,-1.53373942709063,339.675081300838));
#46709=CARTESIAN_POINT('Ctrl Pts',(185.139162997758,-1.39966974248112,339.714881512242));
#46710=CARTESIAN_POINT('Ctrl Pts',(185.13155580986,-1.27042601706156,339.753249079148));
#46711=CARTESIAN_POINT('Ctrl Pts',(185.123948621962,-1.13953589971074,339.786318319177));
#46712=CARTESIAN_POINT('Ctrl Pts',(185.116341434065,-1.00748186865543,339.813955062818));
#46713=CARTESIAN_POINT('Ctrl Pts',(185.108735312539,-0.875446348877749,
339.841587932352));
#46714=CARTESIAN_POINT('Ctrl Pts',(185.101129191014,-0.742247636966592,
339.8637897361));
#46715=CARTESIAN_POINT('Ctrl Pts',(185.093523069488,-0.608379719212441,
339.88047714673));
#46716=CARTESIAN_POINT('Ctrl Pts',(185.085916236046,-0.47449927169694,339.897166119266));
#46717=CARTESIAN_POINT('Ctrl Pts',(185.078309402603,-0.339949896725272,
339.908339622693));
#46718=CARTESIAN_POINT('Ctrl Pts',(185.07070256916,-0.205231435088321,339.913966129366));
#46719=CARTESIAN_POINT('Ctrl Pts',(185.063093244994,-0.0704688622632049,
339.919594478338));
#46720=CARTESIAN_POINT('Ctrl Pts',(185.055483920828,0.0644625019824259,
339.919672203098));
#46721=CARTESIAN_POINT('Ctrl Pts',(185.047874596661,0.199062687180237,339.914219888148));
#46722=CARTESIAN_POINT('Ctrl Pts',(185.040256878758,0.333811347922438,339.908761558828));
#46723=CARTESIAN_POINT('Ctrl Pts',(185.032639160855,0.468227695011502,339.897761033209));
#46724=CARTESIAN_POINT('Ctrl Pts',(185.025021442952,0.601816548656929,339.881290803083));
#46725=CARTESIAN_POINT('Ctrl Pts',(185.017398721146,0.735493153717287,339.864809754045));
#46726=CARTESIAN_POINT('Ctrl Pts',(185.009775999341,0.868340784862089,339.842851917027));
#46727=CARTESIAN_POINT('Ctrl Pts',(185.002153277536,0.999875724090086,339.815540634121));
#46728=CARTESIAN_POINT('Ctrl Pts',(184.994519720211,1.13159763714151,339.788190528869));
#46729=CARTESIAN_POINT('Ctrl Pts',(184.986886162886,1.26200274453607,339.755471894781));
#46730=CARTESIAN_POINT('Ctrl Pts',(184.979252605561,1.39062354056651,339.717557549296));
#46731=CARTESIAN_POINT('Ctrl Pts',(184.977317388195,1.42323077563327,339.707945713467));
#46732=CARTESIAN_POINT('Ctrl Pts',(184.975382170829,1.45572344117559,339.698000189718));
#46733=CARTESIAN_POINT('Ctrl Pts',(184.973446953463,1.48809415044879,339.687724273238));
#46734=CARTESIAN_POINT('Ctrl Pts',(184.96565848958,1.61837310746679,339.646367883108));
#46735=CARTESIAN_POINT('Ctrl Pts',(184.957870025698,1.74712778550745,339.599512591787));
#46736=CARTESIAN_POINT('Ctrl Pts',(184.950081561815,1.87386032935745,339.547288260993));
#46737=CARTESIAN_POINT('Ctrl Pts',(184.942302612285,2.00043805729286,339.49512772721));
#46738=CARTESIAN_POINT('Ctrl Pts',(184.934523662756,2.12499820984358,339.437611352051));
#46739=CARTESIAN_POINT('Ctrl Pts',(184.926744713226,2.24705760125291,339.374918879151));
#46740=CARTESIAN_POINT('Ctrl Pts',(184.918973425117,2.36899677741104,339.312288151532));
#46741=CARTESIAN_POINT('Ctrl Pts',(184.911202137008,2.48843975011919,339.244491648805));
#46742=CARTESIAN_POINT('Ctrl Pts',(184.903430848899,2.60492317208862,339.171757223283));
#46743=CARTESIAN_POINT('Ctrl Pts',(184.89566537582,2.72131943289969,339.099077222817));
#46744=CARTESIAN_POINT('Ctrl Pts',(184.88789990274,2.83476022230911,339.021466860022));
#46745=CARTESIAN_POINT('Ctrl Pts',(184.88013442966,2.94480698156192,338.939199779631));
#46746=CARTESIAN_POINT('Ctrl Pts',(184.872372254371,3.05480700686631,338.856967635894));
#46747=CARTESIAN_POINT('Ctrl Pts',(184.864610079082,3.1614155579396,338.770082940957));
#46748=CARTESIAN_POINT('Ctrl Pts',(184.856847903794,3.26422343308172,338.678862384137));
#46749=CARTESIAN_POINT('Ctrl Pts',(184.849087352215,3.367009802633,338.587660909046));
#46750=CARTESIAN_POINT('Ctrl Pts',(184.841326800636,3.46599678677146,338.492125634548));
#46751=CARTESIAN_POINT('Ctrl Pts',(184.833566249057,3.5608089294898,338.39261297972));
#46752=CARTESIAN_POINT('Ctrl Pts',(184.825805657541,3.65562156012198,338.293099812789));
#46753=CARTESIAN_POINT('Ctrl Pts',(184.818045066026,3.74625903790054,338.189609506535));
#46754=CARTESIAN_POINT('Ctrl Pts',(184.81028447451,3.83238365846775,338.082534437246));
#46755=CARTESIAN_POINT('Ctrl Pts',(184.802522179749,3.91852718112861,337.97543586779));
#46756=CARTESIAN_POINT('Ctrl Pts',(184.794759884987,4.00015563160498,337.864751272943));
#46757=CARTESIAN_POINT('Ctrl Pts',(184.786997590225,4.07697263100072,337.750904801801));
#46758=CARTESIAN_POINT('Ctrl Pts',(184.779227208787,4.15386965753146,337.636939726613));
#46759=CARTESIAN_POINT('Ctrl Pts',(184.771456827349,4.22594500175642,337.519806518169));
#46760=CARTESIAN_POINT('Ctrl Pts',(184.763686445911,4.29294626376753,337.399957382727));
#46761=CARTESIAN_POINT('Ctrl Pts',(184.755911974034,4.35998279619555,337.280045156996));
#46762=CARTESIAN_POINT('Ctrl Pts',(184.748137502157,4.42193974796744,337.157414502478));
#46763=CARTESIAN_POINT('Ctrl Pts',(184.740363030279,4.47861191896625,337.032539874589));
#46764=CARTESIAN_POINT('Ctrl Pts',(184.732576370516,4.53537293380594,336.907469483217));
#46765=CARTESIAN_POINT('Ctrl Pts',(184.724789710753,4.5868324660391,336.780148449852));
#46766=CARTESIAN_POINT('Ctrl Pts',(184.717003050991,4.63283415774104,336.651069571329));
#46767=CARTESIAN_POINT('Ctrl Pts',(184.70973834039,4.6757523007587,336.530643005173));
#46768=CARTESIAN_POINT('Ctrl Pts',(184.70247362979,4.71392020384367,336.40868675833));
#46769=CARTESIAN_POINT('Ctrl Pts',(184.69520891919,4.74725098005436,336.285609269908));
#46770=CARTESIAN_POINT('Ctrl Pts',(184.687424242118,4.78296738276084,336.153722598179));
#46771=CARTESIAN_POINT('Ctrl Pts',(184.679639565047,4.81323836545848,336.020144099434));
#46772=CARTESIAN_POINT('Ctrl Pts',(184.671854887975,4.8379041263559,335.885362483217));
#46773=CARTESIAN_POINT('Ctrl Pts',(184.664079600278,4.86254013700524,335.750743431883));
#46774=CARTESIAN_POINT('Ctrl Pts',(184.656304312581,4.88158430898547,335.61492453046));
#46775=CARTESIAN_POINT('Ctrl Pts',(184.648529024885,4.89492673991659,335.478409106675));
#46776=CARTESIAN_POINT('Ctrl Pts',(184.640761269935,4.9082562446166,335.342025939892));
#46777=CARTESIAN_POINT('Ctrl Pts',(184.632993514986,4.91589496413867,335.204947979227));
#46778=CARTESIAN_POINT('Ctrl Pts',(184.625225760037,4.91778419782772,335.067687857818));
#46779=CARTESIAN_POINT('Ctrl Pts',(184.617463687663,4.91967204942996,334.930528150351));
#46780=CARTESIAN_POINT('Ctrl Pts',(184.609701615289,4.91581878241357,334.793186935617));
#46781=CARTESIAN_POINT('Ctrl Pts',(184.601939542914,4.90621762379767,334.65618072998));
#46782=CARTESIAN_POINT('Ctrl Pts',(184.594180552715,4.89662027762425,334.519228926973));
#46783=CARTESIAN_POINT('Ctrl Pts',(184.586421562516,4.88127960618991,334.382612256533));
#46784=CARTESIAN_POINT('Ctrl Pts',(184.578662572317,4.86024092128453,334.246845799606));
#46785=CARTESIAN_POINT('Ctrl Pts',(184.570905073578,4.83920628050715,334.111105440172));
#46786=CARTESIAN_POINT('Ctrl Pts',(184.563147574839,4.81247586460318,333.976215354093));
#46787=CARTESIAN_POINT('Ctrl Pts',(184.555390076099,4.78014665025893,333.842683680009));
#46788=CARTESIAN_POINT('Ctrl Pts',(184.547632401474,4.74781670291267,333.709148978354));
#46789=CARTESIAN_POINT('Ctrl Pts',(184.539874726848,4.70988779598382,333.576973128845));
#46790=CARTESIAN_POINT('Ctrl Pts',(184.532117052223,4.66650755751355,333.446651913392));
#46791=CARTESIAN_POINT('Ctrl Pts',(184.524357534611,4.62311701322361,333.316299737599));
#46792=CARTESIAN_POINT('Ctrl Pts',(184.516598016999,4.57427268320736,333.187803442396));
#46793=CARTESIAN_POINT('Ctrl Pts',(184.508838499386,4.52017125212072,333.061641180276));
#46794=CARTESIAN_POINT('Ctrl Pts',(184.501070656481,4.46601177486198,332.935343556924));
#46795=CARTESIAN_POINT('Ctrl Pts',(184.493302813575,4.40658408313757,332.811385327803));
#46796=CARTESIAN_POINT('Ctrl Pts',(184.48553497067,4.34213222882723,332.690222787826));
#46797=CARTESIAN_POINT('Ctrl Pts',(184.47776291104,4.27764538723547,332.56899447553));
#46798=CARTESIAN_POINT('Ctrl Pts',(184.46999085141,4.2081291455521,332.450565212436));
#46799=CARTESIAN_POINT('Ctrl Pts',(184.46221879178,4.13387175970386,332.335363563857));
#46800=CARTESIAN_POINT('Ctrl Pts',(184.454434302843,4.05949561925503,332.219977681405));
#46801=CARTESIAN_POINT('Ctrl Pts',(184.446649813906,3.98036340801068,332.107830046665));
#46802=CARTESIAN_POINT('Ctrl Pts',(184.438865324969,3.89680519102534,331.999318016567));
#46803=CARTESIAN_POINT('Ctrl Pts',(184.431567178284,3.81846734133424,331.897585363452));
#46804=CARTESIAN_POINT('Ctrl Pts',(184.4242690316,3.73623980330836,331.799048106545));
#46805=CARTESIAN_POINT('Ctrl Pts',(184.416970884915,3.65042360366862,331.704003856756));
#46806=CARTESIAN_POINT('Ctrl Pts',(184.409204894486,3.55910620297908,331.602866846755));
#46807=CARTESIAN_POINT('Ctrl Pts',(184.401438904057,3.46343492066193,331.50536424042));
#46808=CARTESIAN_POINT('Ctrl Pts',(184.393672913627,3.3637306636303,331.411894777873));
#46809=CARTESIAN_POINT('Ctrl Pts',(184.385916602342,3.26415067302245,331.318541811013));
#46810=CARTESIAN_POINT('Ctrl Pts',(184.378160291057,3.16054799150972,331.229212252213));
#46811=CARTESIAN_POINT('Ctrl Pts',(184.370403979771,3.05328302497456,331.144271037547));
#46812=CARTESIAN_POINT('Ctrl Pts',(184.362655469153,2.94612593681738,331.059415249844));
#46813=CARTESIAN_POINT('Ctrl Pts',(184.354906958534,2.83531419825708,330.978939265473));
#46814=CARTESIAN_POINT('Ctrl Pts',(184.347158447916,2.72124395620983,330.90317020206));
#46815=CARTESIAN_POINT('Ctrl Pts',(184.339415866339,2.60726099896148,330.827459115971));
#46816=CARTESIAN_POINT('Ctrl Pts',(184.331673284762,2.49002482595842,330.756447998258));
#46817=CARTESIAN_POINT('Ctrl Pts',(184.323930703185,2.36996315621844,330.69042256124));
#46818=CARTESIAN_POINT('Ctrl Pts',(184.316191510396,2.2499540352959,330.62442602236));
#46819=CARTESIAN_POINT('Ctrl Pts',(184.308452317607,2.12712221996486,330.563411012492));
#46820=CARTESIAN_POINT('Ctrl Pts',(184.300713124817,2.00192259021132,330.507618782282));
#46821=CARTESIAN_POINT('Ctrl Pts',(184.292975607458,1.87675006448171,330.451838630335));
#46822=CARTESIAN_POINT('Ctrl Pts',(184.285238090099,1.74921110162522,330.40127916862));
#46823=CARTESIAN_POINT('Ctrl Pts',(184.277500572741,1.61978288774046,330.356134534778));
#46824=CARTESIAN_POINT('Ctrl Pts',(184.269763044928,1.49035449899087,330.310989839942));
#46825=CARTESIAN_POINT('Ctrl Pts',(184.262025517115,1.35903722411994,330.271260116828));
#46826=CARTESIAN_POINT('Ctrl Pts',(184.254287989302,1.2263254346455,330.237090281053));
#46827=CARTESIAN_POINT('Ctrl Pts',(184.246548765495,1.09358455597324,330.202912955565));
#46828=CARTESIAN_POINT('Ctrl Pts',(184.238809541688,0.959448933976456,330.174298039999));
#46829=CARTESIAN_POINT('Ctrl Pts',(184.23107031788,0.824424805284255,330.15133968988));
#46830=CARTESIAN_POINT('Ctrl Pts',(184.223322887694,0.689257502135376,330.128356995599));
#46831=CARTESIAN_POINT('Ctrl Pts',(184.215575457508,0.553200197285356,330.11104291412));
#46832=CARTESIAN_POINT('Ctrl Pts',(184.207828027322,0.416766496517759,330.099439955487));
#46833=CARTESIAN_POINT('Ctrl Pts',(184.200076477443,0.280260247199368,330.087830826986));
#46834=CARTESIAN_POINT('Ctrl Pts',(184.192324927565,0.143377594536541,330.081938889113));
#46835=CARTESIAN_POINT('Ctrl Pts',(184.184573377687,0.00663283769598015,
330.081754472582));
#46836=CARTESIAN_POINT('Ctrl Pts',(184.176809358013,-0.130331898273189,
330.081569759384));
#46837=CARTESIAN_POINT('Ctrl Pts',(184.169045338339,-0.267157903322725,
330.087110899134));
#46838=CARTESIAN_POINT('Ctrl Pts',(184.161281318665,-0.403334414585777,
330.098316165591));
#46839=CARTESIAN_POINT('Ctrl Pts',(184.153765162657,-0.535163537412979,
330.109163707757));
#46840=CARTESIAN_POINT('Ctrl Pts',(184.146249006649,-0.66638369400634,330.125319154275));
#46841=CARTESIAN_POINT('Ctrl Pts',(184.138732850642,-0.796541975815797,
330.146681141398));
#46842=CARTESIAN_POINT('Ctrl Pts',(184.1309552338,-0.931228009951312,330.168786237492));
#46843=CARTESIAN_POINT('Ctrl Pts',(184.123177616959,-1.06520495165966,330.196536910097));
#46844=CARTESIAN_POINT('Ctrl Pts',(184.115400000118,-1.19796258057449,330.229877494441));
#46845=CARTESIAN_POINT('Ctrl Pts',(184.107631935139,-1.33055716692858,330.26317713248));
#46846=CARTESIAN_POINT('Ctrl Pts',(184.09986387016,-1.46193504483815,330.30205292825));
#46847=CARTESIAN_POINT('Ctrl Pts',(184.092095805181,-1.59159321286036,330.346397727859));
#46848=CARTESIAN_POINT('Ctrl Pts',(184.084335426717,-1.72112308386848,330.3906986482));
#46849=CARTESIAN_POINT('Ctrl Pts',(184.076575048254,-1.84893626423228,330.440457677262));
#46850=CARTESIAN_POINT('Ctrl Pts',(184.06881466979,-1.97454236023251,330.495517173954));
#46851=CARTESIAN_POINT('Ctrl Pts',(184.061060119138,-2.10005412982255,330.550535322614));
#46852=CARTESIAN_POINT('Ctrl Pts',(184.053305568486,-2.22336175788803,330.610845859634));
#46853=CARTESIAN_POINT('Ctrl Pts',(184.045551017834,-2.3439927091478,330.67624223135));
#46854=CARTESIAN_POINT('Ctrl Pts',(184.037799743937,-2.46457268671841,330.741610969244));
#46855=CARTESIAN_POINT('Ctrl Pts',(184.03004847004,-2.58247789444863,330.812061081661));
#46856=CARTESIAN_POINT('Ctrl Pts',(184.022297196143,-2.69725858685646,330.887339160819));
#46857=CARTESIAN_POINT('Ctrl Pts',(184.014547531043,-2.81201545622994,330.962601615814));
#46858=CARTESIAN_POINT('Ctrl Pts',(184.006797865943,-2.92364877381903,331.042689830283));
#46859=CARTESIAN_POINT('Ctrl Pts',(183.999048200843,-3.03173642524737,331.127306194607));
#46860=CARTESIAN_POINT('Ctrl Pts',(183.991298469927,-3.1398249946362,331.211923277557));
#46861=CARTESIAN_POINT('Ctrl Pts',(183.983548739011,-3.24436753026002,331.301068346297));
#46862=CARTESIAN_POINT('Ctrl Pts',(183.975799008096,-3.34497407275734,331.394402751959));
#46863=CARTESIAN_POINT('Ctrl Pts',(183.968047537065,-3.44560320531852,331.487758114809));
#46864=CARTESIAN_POINT('Ctrl Pts',(183.960296066035,-3.54229429981986,331.585304420843));
#46865=CARTESIAN_POINT('Ctrl Pts',(183.952544595004,-3.63469370544349,331.686665617522));
#46866=CARTESIAN_POINT('Ctrl Pts',(183.944784916504,-3.72719094609492,331.78813413822));
#46867=CARTESIAN_POINT('Ctrl Pts',(183.937025238003,-3.81538715692437,331.893425329381));
#46868=CARTESIAN_POINT('Ctrl Pts',(183.929265559502,-3.89896816031605,332.002129030905));
#46869=CARTESIAN_POINT('Ctrl Pts',(183.921501741213,-3.98259375416966,332.110890725849));
#46870=CARTESIAN_POINT('Ctrl Pts',(183.913737922924,-4.0615990095167,332.223068239711));
#46871=CARTESIAN_POINT('Ctrl Pts',(183.905974104635,-4.13571326520763,332.338222614401));
#46872=CARTESIAN_POINT('Ctrl Pts',(183.898197906043,-4.2099457046265,332.453560616021));
#46873=CARTESIAN_POINT('Ctrl Pts',(183.89042170745,-4.27927136155874,332.571884627123));
#46874=CARTESIAN_POINT('Ctrl Pts',(183.882645508857,-4.34346527456366,332.692730516138));
#46875=CARTESIAN_POINT('Ctrl Pts',(183.875261944694,-4.40441791998991,332.807474676131));
#46876=CARTESIAN_POINT('Ctrl Pts',(183.867878380531,-4.46074422753017,332.924492031672));
#46877=CARTESIAN_POINT('Ctrl Pts',(183.860494816367,-4.51229256241462,333.043370527239));
#46878=CARTESIAN_POINT('Ctrl Pts',(183.851901462611,-4.57228704034016,333.181727145238));
#46879=CARTESIAN_POINT('Ctrl Pts',(183.843308108854,-4.62597157335744,333.322977368862));
#46880=CARTESIAN_POINT('Ctrl Pts',(183.834714755098,-4.67308623617143,333.466556785595));
#46881=CARTESIAN_POINT('Ctrl Pts',(183.826155630823,-4.72001322947433,333.609564289524));
#46882=CARTESIAN_POINT('Ctrl Pts',(183.817596506549,-4.76042246392151,333.754882245335));
#46883=CARTESIAN_POINT('Ctrl Pts',(183.809037382274,-4.79410300807903,333.901929232505));
#46884=CARTESIAN_POINT('Ctrl Pts',(183.800500556196,-4.82769580781691,334.048593133448));
#46885=CARTESIAN_POINT('Ctrl Pts',(183.791963730118,-4.85459480847109,334.196976842495));
#46886=CARTESIAN_POINT('Ctrl Pts',(183.78342690404,-4.87463832611427,334.346483166186));
#46887=CARTESIAN_POINT('Ctrl Pts',(183.77492515661,-4.89459948299498,334.495375153859));
#46888=CARTESIAN_POINT('Ctrl Pts',(183.766423409181,-4.90776128352893,334.645380310851));
#46889=CARTESIAN_POINT('Ctrl Pts',(183.757921661751,-4.9140129244875,334.795892086215));
#46890=CARTESIAN_POINT('Ctrl Pts',(183.754126524013,-4.91680362589586,334.863079793613));
#46891=CARTESIAN_POINT('Ctrl Pts',(183.750331386275,-4.91821801072524,334.930368253243));
#46892=CARTESIAN_POINT('Ctrl Pts',(183.746536248537,-4.91824946343417,334.997702625515));
#46893=CARTESIAN_POINT('',(185.231676812499,2.85706463458485,339.00329423554));
#46894=CARTESIAN_POINT('Origin',(185.231676812499,0.,335.));
#46895=CARTESIAN_POINT('',(184.091817376473,-4.91824940656917,334.997583953229));
#46896=CARTESIAN_POINT('Ctrl Pts',(185.231676812499,2.85706463458463,339.00329423554));
#46897=CARTESIAN_POINT('Ctrl Pts',(185.222579442691,2.9878247153018,338.909973590028));
#46898=CARTESIAN_POINT('Ctrl Pts',(185.213482072884,3.11390580132401,338.810317313122));
#46899=CARTESIAN_POINT('Ctrl Pts',(185.204384703076,3.23476879094588,338.704787973909));
#46900=CARTESIAN_POINT('Ctrl Pts',(185.1950657941,3.3585750363445,338.596688784007));
#46901=CARTESIAN_POINT('Ctrl Pts',(185.185746885124,3.476905728084,338.48242695956));
#46902=CARTESIAN_POINT('Ctrl Pts',(185.176427976148,3.58922166565946,338.362539352522));
#46903=CARTESIAN_POINT('Ctrl Pts',(185.167314876684,3.69905708878743,338.245299481396));
#46904=CARTESIAN_POINT('Ctrl Pts',(185.15820177722,3.80314056875857,338.122679795787));
#46905=CARTESIAN_POINT('Ctrl Pts',(185.149088677757,3.90100650166295,337.995218078285));
#46906=CARTESIAN_POINT('Ctrl Pts',(185.139666864024,4.00218772921781,337.863438482869));
#46907=CARTESIAN_POINT('Ctrl Pts',(185.130245050292,4.09672267977152,337.726483109028));
#46908=CARTESIAN_POINT('Ctrl Pts',(185.120823236559,4.18414116197834,337.584984680639));
#46909=CARTESIAN_POINT('Ctrl Pts',(185.111401422827,4.27155964418516,337.44348625225));
#46910=CARTESIAN_POINT('Ctrl Pts',(185.101979609095,4.35186152211415,337.297444838005));
#46911=CARTESIAN_POINT('Ctrl Pts',(185.092557795362,4.424623503881,337.147531120008));
#46912=CARTESIAN_POINT('Ctrl Pts',(185.084782311257,4.48467135122184,337.023812718805));
#46913=CARTESIAN_POINT('Ctrl Pts',(185.077006827152,4.53954842512907,336.897528290713));
#46914=CARTESIAN_POINT('Ctrl Pts',(185.069231343047,4.58904037605888,336.769149934121));
#46915=CARTESIAN_POINT('Ctrl Pts',(185.061456840608,4.63852607856139,336.640787785475));
#46916=CARTESIAN_POINT('Ctrl Pts',(185.053682338168,4.68262787275381,336.510332596953));
#46917=CARTESIAN_POINT('Ctrl Pts',(185.045907835729,4.72117985492044,336.378275676341));
#46918=CARTESIAN_POINT('Ctrl Pts',(185.038129436014,4.75975116278613,336.246152556998));
#46919=CARTESIAN_POINT('Ctrl Pts',(185.030351036299,4.79276698724958,336.112426473256));
#46920=CARTESIAN_POINT('Ctrl Pts',(185.022572636584,4.82011148302006,335.977603372416));
#46921=CARTESIAN_POINT('Ctrl Pts',(185.014792468078,4.84746219687077,335.842749613089));
#46922=CARTESIAN_POINT('Ctrl Pts',(185.007012299572,4.86913894489199,335.706798722194));
#46923=CARTESIAN_POINT('Ctrl Pts',(184.999232131065,4.88507734499522,335.570265197881));
#46924=CARTESIAN_POINT('Ctrl Pts',(184.991443525169,4.90103302987852,335.433583606515));
#46925=CARTESIAN_POINT('Ctrl Pts',(184.983654919272,4.91123789581269,335.296318506361));
#46926=CARTESIAN_POINT('Ctrl Pts',(184.975866313375,4.91567957915306,335.158988482594));
#46927=CARTESIAN_POINT('Ctrl Pts',(184.968390468325,4.91994290135146,335.027173111266));
#46928=CARTESIAN_POINT('Ctrl Pts',(184.960914623275,4.91889694997854,334.895298241123));
#46929=CARTESIAN_POINT('Ctrl Pts',(184.953438778225,4.9125758885357,334.76381955653));
#46930=CARTESIAN_POINT('Ctrl Pts',(184.945564587241,4.90591801311239,334.625335108822));
#46931=CARTESIAN_POINT('Ctrl Pts',(184.937690396256,4.89339311908122,334.486988322013));
#46932=CARTESIAN_POINT('Ctrl Pts',(184.929816205271,4.87501593909813,334.349306019669));
#46933=CARTESIAN_POINT('Ctrl Pts',(184.921949019059,4.85665510720187,334.21174619761));
#46934=CARTESIAN_POINT('Ctrl Pts',(184.914081832846,4.83245240543065,334.074850055284));
#46935=CARTESIAN_POINT('Ctrl Pts',(184.906214646633,4.8024745030993,333.939141051043));
#46936=CARTESIAN_POINT('Ctrl Pts',(184.898352758719,4.77251678992486,333.80352344247));
#46937=CARTESIAN_POINT('Ctrl Pts',(184.890490870804,4.73679170318165,333.66909174716));
#46938=CARTESIAN_POINT('Ctrl Pts',(184.882628982889,4.69541726479236,333.536360778064));
#46939=CARTESIAN_POINT('Ctrl Pts',(184.874770691361,4.6540617529575,333.403690526165));
#46940=CARTESIAN_POINT('Ctrl Pts',(184.866912399832,4.60706214927302,333.272719810437));
#46941=CARTESIAN_POINT('Ctrl Pts',(184.859054108303,4.55458669943747,333.143949607417));
#46942=CARTESIAN_POINT('Ctrl Pts',(184.851196167121,4.50211358911507,333.01518514536));
#46943=CARTESIAN_POINT('Ctrl Pts',(184.843338225938,4.44416525229962,332.888621353558));
#46944=CARTESIAN_POINT('Ctrl Pts',(184.835480284756,4.38095863009341,332.764740609256));
#46945=CARTESIAN_POINT('Ctrl Pts',(184.827622207873,4.31775091636225,332.640857725638));
#46946=CARTESIAN_POINT('Ctrl Pts',(184.819764130991,4.24928490721179,332.519658318505));
#46947=CARTESIAN_POINT('Ctrl Pts',(184.811906054108,4.17582400184014,332.401601076017));
#46948=CARTESIAN_POINT('Ctrl Pts',(184.804046302178,4.10234743734809,332.283518668136));
#46949=CARTESIAN_POINT('Ctrl Pts',(184.796186550247,4.02387405542442,332.168580079521));
#46950=CARTESIAN_POINT('Ctrl Pts',(184.788326798316,3.94071103870938,332.057215676966));
#46951=CARTESIAN_POINT('Ctrl Pts',(184.780463831184,3.85751400236523,331.945805718396));
#46952=CARTESIAN_POINT('Ctrl Pts',(184.772600864051,3.76962373634181,331.837973160097));
#46953=CARTESIAN_POINT('Ctrl Pts',(184.764737896919,3.67738806029112,331.734115722116));
#46954=CARTESIAN_POINT('Ctrl Pts',(184.756865106111,3.58503714868493,331.630128528817));
#46955=CARTESIAN_POINT('Ctrl Pts',(184.748992315303,3.48833023282654,331.530126659555));
#46956=CARTESIAN_POINT('Ctrl Pts',(184.741119524495,3.38765294139393,331.434471902906));
#46957=CARTESIAN_POINT('Ctrl Pts',(184.733241550299,3.28690936477144,331.338754167867));
#46958=CARTESIAN_POINT('Ctrl Pts',(184.725363576103,3.18219048574338,331.247389498811));
#46959=CARTESIAN_POINT('Ctrl Pts',(184.717485601907,3.07391490856393,331.160699256712));
#46960=CARTESIAN_POINT('Ctrl Pts',(184.70959467446,2.96546130074035,331.073866475363));
#46961=CARTESIAN_POINT('Ctrl Pts',(184.701703747012,2.85343961281812,330.991723703143));
#46962=CARTESIAN_POINT('Ctrl Pts',(184.693812819564,2.7382981212166,330.914549417525));
#46963=CARTESIAN_POINT('Ctrl Pts',(184.68760879436,2.64777128255249,330.85387325287));
#46964=CARTESIAN_POINT('Ctrl Pts',(184.681404769155,2.5553165529785,330.796267481384));
#46965=CARTESIAN_POINT('Ctrl Pts',(184.675200743951,2.4611617124476,330.741847103769));
#46966=CARTESIAN_POINT('Ctrl Pts',(184.667489928554,2.34413920364659,330.674209485963));
#46967=CARTESIAN_POINT('Ctrl Pts',(184.659779113157,2.22411053131831,330.611274870948));
#46968=CARTESIAN_POINT('Ctrl Pts',(184.65206829776,2.10149395557967,330.553326387381));
#46969=CARTESIAN_POINT('Ctrl Pts',(184.644367804453,1.97904152063397,330.495455476605));
#46970=CARTESIAN_POINT('Ctrl Pts',(184.636667311146,1.85400842801085,330.442557590228));
#46971=CARTESIAN_POINT('Ctrl Pts',(184.628966817839,1.7268408492561,330.394872016562));
#46972=CARTESIAN_POINT('Ctrl Pts',(184.621274712016,1.59981178319868,330.347238382687));
#46973=CARTESIAN_POINT('Ctrl Pts',(184.613582606194,1.47065322559616,330.304805906676));
#46974=CARTESIAN_POINT('Ctrl Pts',(184.605890500372,1.3398344216355,330.267767251592));
#46975=CARTESIAN_POINT('Ctrl Pts',(184.598204855771,1.20912550296542,330.23075970827));
#46976=CARTESIAN_POINT('Ctrl Pts',(184.59051921117,1.0767594938103,330.199137079345));
#46977=CARTESIAN_POINT('Ctrl Pts',(184.582833566569,0.943223598027069,330.173043162962));
#46978=CARTESIAN_POINT('Ctrl Pts',(184.575088947532,0.808663038133427,330.146749019522));
#46979=CARTESIAN_POINT('Ctrl Pts',(184.567344328495,0.672914944454686,330.126068941496));
#46980=CARTESIAN_POINT('Ctrl Pts',(184.559599709458,0.536491694095676,330.111098311004));
#46981=CARTESIAN_POINT('Ctrl Pts',(184.55192014685,0.401214427747725,330.096253436958));
#46982=CARTESIAN_POINT('Ctrl Pts',(184.544240584243,0.265273708744855,330.087022482791));
#46983=CARTESIAN_POINT('Ctrl Pts',(184.536561021635,0.129176771301089,330.083446692625));
#46984=CARTESIAN_POINT('Ctrl Pts',(184.528881768299,-0.00691468524943978,
330.079871046464));
#46985=CARTESIAN_POINT('Ctrl Pts',(184.521202514962,-0.143161949681559,
330.081950121998));
#46986=CARTESIAN_POINT('Ctrl Pts',(184.513523261626,-0.279056173881734,
330.089673054234));
#46987=CARTESIAN_POINT('Ctrl Pts',(184.50584258536,-0.414975578638653,330.097397417492));
#46988=CARTESIAN_POINT('Ctrl Pts',(184.498161909095,-0.550541415532521,
330.110767694871));
#46989=CARTESIAN_POINT('Ctrl Pts',(184.490481232829,-0.685248845503751,
330.129721046774));
#46990=CARTESIAN_POINT('Ctrl Pts',(184.482688022566,-0.821929951359796,
330.148952095116));
#46991=CARTESIAN_POINT('Ctrl Pts',(184.474894812304,-0.957726877239136,
330.17393105805));
#46992=CARTESIAN_POINT('Ctrl Pts',(184.467101602041,-1.09212301522409,330.204538564213));
#46993=CARTESIAN_POINT('Ctrl Pts',(184.459408829424,-1.22478707731167,330.23475160574));
#46994=CARTESIAN_POINT('Ctrl Pts',(184.451716056807,-1.35608587604265,330.270448800903));
#46995=CARTESIAN_POINT('Ctrl Pts',(184.444023284189,-1.48553870176006,330.311465279208));
#46996=CARTESIAN_POINT('Ctrl Pts',(184.436179855104,-1.61752675196568,330.353285030671));
#46997=CARTESIAN_POINT('Ctrl Pts',(184.428336426019,-1.74759536268877,330.400634423609));
#46998=CARTESIAN_POINT('Ctrl Pts',(184.420492996933,-1.87525817414061,330.453288018489));
#46999=CARTESIAN_POINT('Ctrl Pts',(184.412649567848,-2.00292098559246,330.505941613368));
#47000=CARTESIAN_POINT('Ctrl Pts',(184.404806138762,-2.12817763568885,330.563899166777));
#47001=CARTESIAN_POINT('Ctrl Pts',(184.396962709677,-2.25057076624572,330.626887345538));
#47002=CARTESIAN_POINT('Ctrl Pts',(184.389174245794,-2.37210618990496,330.689434115576));
#47003=CARTESIAN_POINT('Ctrl Pts',(184.381385781912,-2.49121980444608,330.757147720362));
#47004=CARTESIAN_POINT('Ctrl Pts',(184.373597318029,-2.60744245830814,330.82981692379));
#47005=CARTESIAN_POINT('Ctrl Pts',(184.365818368499,-2.72352313509079,330.90239735484));
#47006=CARTESIAN_POINT('Ctrl Pts',(184.358039418969,-2.83671955153112,330.979921133902));
#47007=CARTESIAN_POINT('Ctrl Pts',(184.35026046944,-2.94658535540073,331.06213029598));
#47008=CARTESIAN_POINT('Ctrl Pts',(184.342489181331,-3.05634295337928,331.144258490957));
#47009=CARTESIAN_POINT('Ctrl Pts',(184.334717893222,-3.16277615748277,331.23106265316));
#47010=CARTESIAN_POINT('Ctrl Pts',(184.326946605113,-3.26546621479366,331.322240700842));
#47011=CARTESIAN_POINT('Ctrl Pts',(184.319181132033,-3.36807943212012,331.413350522643));
#47012=CARTESIAN_POINT('Ctrl Pts',(184.311415658953,-3.4669547881139,331.508827457513));
#47013=CARTESIAN_POINT('Ctrl Pts',(184.303650185873,-3.56170562253267,331.608328417886));
#47014=CARTESIAN_POINT('Ctrl Pts',(184.295888010585,-3.65641621877765,331.707787122832));
#47015=CARTESIAN_POINT('Ctrl Pts',(184.288125835296,-3.74700550970919,331.811266172619));
#47016=CARTESIAN_POINT('Ctrl Pts',(184.280363660007,-3.83312297281925,331.918384946534));
#47017=CARTESIAN_POINT('Ctrl Pts',(184.272603108428,-3.91922242167776,332.025481313096));
#47018=CARTESIAN_POINT('Ctrl Pts',(184.264842556849,-4.00085165976164,332.136215585984));
#47019=CARTESIAN_POINT('Ctrl Pts',(184.25708200527,-4.07770007525033,332.250173612971));
#47020=CARTESIAN_POINT('Ctrl Pts',(184.249321413755,-4.15454888620958,332.364132226398));
#47021=CARTESIAN_POINT('Ctrl Pts',(184.241560822239,-4.2266166077965,332.481314304259));
#47022=CARTESIAN_POINT('Ctrl Pts',(184.233800230724,-4.29363585803693,332.601276551772));
#47023=CARTESIAN_POINT('Ctrl Pts',(184.226037935962,-4.36066981724358,332.721265127849));
#47024=CARTESIAN_POINT('Ctrl Pts',(184.2182756412,-4.42265291031737,332.844034748019));
#47025=CARTESIAN_POINT('Ctrl Pts',(184.210513346439,-4.4793638093941,332.96911769775));
#47026=CARTESIAN_POINT('Ctrl Pts',(184.202742965001,-4.53613378928388,333.094330957572));
#47027=CARTESIAN_POINT('Ctrl Pts',(184.194972583563,-4.58762044218239,333.221862006101));
#47028=CARTESIAN_POINT('Ctrl Pts',(184.187202202125,-4.6336504895927,333.351222815903));
#47029=CARTESIAN_POINT('Ctrl Pts',(184.179427730247,-4.67970476787436,333.480651723075));
#47030=CARTESIAN_POINT('Ctrl Pts',(184.17165325837,-4.72029660145657,333.611911939237));
#47031=CARTESIAN_POINT('Ctrl Pts',(184.163878786493,-4.75530296609509,333.744501388632));
#47032=CARTESIAN_POINT('Ctrl Pts',(184.15609212673,-4.79036420951869,333.877298695883));
#47033=CARTESIAN_POINT('Ctrl Pts',(184.148305466967,-4.81982240259727,334.011429020029));
#47034=CARTESIAN_POINT('Ctrl Pts',(184.140518807204,-4.84360574158947,334.146380364248));
#47035=CARTESIAN_POINT('Ctrl Pts',(184.133254096604,-4.86579485478363,334.272285757665));
#47036=CARTESIAN_POINT('Ctrl Pts',(184.125989386003,-4.88304489384078,334.398905468304));
#47037=CARTESIAN_POINT('Ctrl Pts',(184.118724675403,-4.89533845131523,334.525822280601));
#47038=CARTESIAN_POINT('Ctrl Pts',(184.109755575772,-4.91051622616177,334.682515313133));
#47039=CARTESIAN_POINT('Ctrl Pts',(184.10078647614,-4.91817196805098,334.839945510906));
#47040=CARTESIAN_POINT('Ctrl Pts',(184.091817376508,-4.91824940656887,334.997583952616));
#47041=CARTESIAN_POINT('',(182.34181737656,-4.91824916970108,334.997142162596));
#47042=CARTESIAN_POINT('Ctrl Pts',(184.091817376473,-4.91824940656917,334.997583953229));
#47043=CARTESIAN_POINT('Ctrl Pts',(184.084130311134,-4.91831577608455,335.132689710906));
#47044=CARTESIAN_POINT('Ctrl Pts',(184.076443245795,-4.91281085209014,335.26801291328));
#47045=CARTESIAN_POINT('Ctrl Pts',(184.068756180455,-4.90170722235522,335.403050082261));
#47046=CARTESIAN_POINT('Ctrl Pts',(184.061077607281,-4.89061585918133,335.537938071045));
#47047=CARTESIAN_POINT('Ctrl Pts',(184.053399034107,-4.87393812510857,335.67254025952));
#47048=CARTESIAN_POINT('Ctrl Pts',(184.045720460933,-4.85169861664758,335.80635202965));
#47049=CARTESIAN_POINT('Ctrl Pts',(184.038048437324,-4.82947807774062,335.940049662832));
#47050=CARTESIAN_POINT('Ctrl Pts',(184.030376413715,-4.80170526764821,336.072957826291));
#47051=CARTESIAN_POINT('Ctrl Pts',(184.022704390106,-4.76845665061498,336.204576371056));
#47052=CARTESIAN_POINT('Ctrl Pts',(184.015036522363,-4.73522604406092,336.336123619229));
#47053=CARTESIAN_POINT('Ctrl Pts',(184.007368654621,-4.69652562755459,336.466382251169));
#47054=CARTESIAN_POINT('Ctrl Pts',(183.999700786879,-4.65248300065029,336.59486206023));
#47055=CARTESIAN_POINT('Ctrl Pts',(183.992035032746,-4.60845251387658,336.723306454471));
#47056=CARTESIAN_POINT('Ctrl Pts',(183.984369278613,-4.55908287407189,336.849972622525));
#47057=CARTESIAN_POINT('Ctrl Pts',(183.97670352448,-4.50455148146989,336.974385730623));
#47058=CARTESIAN_POINT('Ctrl Pts',(183.969038137298,-4.45002269922133,337.098792883213));
#47059=CARTESIAN_POINT('Ctrl Pts',(183.961372750116,-4.39033281619444,337.220946823846));
#47060=CARTESIAN_POINT('Ctrl Pts',(183.953707362934,-4.32570708748705,337.34039339765));
#47061=CARTESIAN_POINT('Ctrl Pts',(183.946040596582,-4.26106973121236,337.459861462478));
#47062=CARTESIAN_POINT('Ctrl Pts',(183.938373830231,-4.19149495373998,337.576620839945));
#47063=CARTESIAN_POINT('Ctrl Pts',(183.93070706388,-4.11725334028815,337.690243110647));
#47064=CARTESIAN_POINT('Ctrl Pts',(183.92303249413,-4.04293616213615,337.803981028524));
#47065=CARTESIAN_POINT('Ctrl Pts',(183.91535792438,-3.96394288019147,337.914575126835));
#47066=CARTESIAN_POINT('Ctrl Pts',(183.90768335463,-3.88058692300308,338.021626746558));
#47067=CARTESIAN_POINT('Ctrl Pts',(183.900004834352,-3.79718805785987,338.128733471715));
#47068=CARTESIAN_POINT('Ctrl Pts',(183.892326314074,-3.70942230367937,338.232293781788));
#47069=CARTESIAN_POINT('Ctrl Pts',(183.884647793795,-3.61764173005681,338.331944083482));
#47070=CARTESIAN_POINT('Ctrl Pts',(183.876957150543,-3.52571625176181,338.431751714704));
#47071=CARTESIAN_POINT('Ctrl Pts',(183.869266507291,-3.42976357394534,338.527636722327));
#47072=CARTESIAN_POINT('Ctrl Pts',(183.861575864039,-3.33017130772584,338.619273701131));
#47073=CARTESIAN_POINT('Ctrl Pts',(183.854546123069,-3.23913759166378,338.703035774492));
#47074=CARTESIAN_POINT('Ctrl Pts',(183.847516382099,-3.14506353565459,338.783248907216));
#47075=CARTESIAN_POINT('Ctrl Pts',(183.84048664113,-3.04826641418166,338.85969622259));
#47076=CARTESIAN_POINT('Ctrl Pts',(183.8327206507,-2.94133139023732,338.944150133776));
#47077=CARTESIAN_POINT('Ctrl Pts',(183.824954660271,-2.83071108871737,339.024293139672));
#47078=CARTESIAN_POINT('Ctrl Pts',(183.817188669842,-2.7167885402977,339.099785737061));
#47079=CARTESIAN_POINT('Ctrl Pts',(183.809432358556,-2.60300797927253,339.175184244233));
#47080=CARTESIAN_POINT('Ctrl Pts',(183.801676047271,-2.48593368351757,339.245943660324));
#47081=CARTESIAN_POINT('Ctrl Pts',(183.793919735985,-2.36598197792825,339.311764411771));
#47082=CARTESIAN_POINT('Ctrl Pts',(183.786171225367,-2.24615091000722,339.377518966061));
#47083=CARTESIAN_POINT('Ctrl Pts',(183.778422714749,-2.12344853218142,339.438344552282));
#47084=CARTESIAN_POINT('Ctrl Pts',(183.77067420413,-1.99832008759991,339.493984856449));
#47085=CARTESIAN_POINT('Ctrl Pts',(183.762931622553,-1.87328738938408,339.54958258551));
#47086=CARTESIAN_POINT('Ctrl Pts',(183.755189040976,-1.74583267588013,339.600002771));
#47087=CARTESIAN_POINT('Ctrl Pts',(183.747446459399,-1.61642539875726,339.645035198225));
#47088=CARTESIAN_POINT('Ctrl Pts',(183.73970726661,-1.48707476085487,339.690047915574));
#47089=CARTESIAN_POINT('Ctrl Pts',(183.731968073821,-1.35577362843123,339.729677436273));
#47090=CARTESIAN_POINT('Ctrl Pts',(183.724228881032,-1.22301080180226,339.763761921127));
#47091=CARTESIAN_POINT('Ctrl Pts',(183.716491363673,-1.09027671652678,339.79783902715));
#47092=CARTESIAN_POINT('Ctrl Pts',(183.708753846314,-0.956081945791869,
339.826373387539));
#47093=CARTESIAN_POINT('Ctrl Pts',(183.701016328955,-0.82092940889344,339.8492533413));
#47094=CARTESIAN_POINT('Ctrl Pts',(183.693278801142,-0.685776689396465,
339.872133325974));
#47095=CARTESIAN_POINT('Ctrl Pts',(183.685541273329,-0.549666587551065,
339.889358823176));
#47096=CARTESIAN_POINT('Ctrl Pts',(183.677803745517,-0.413110740497895,
339.900869573717));
#47097=CARTESIAN_POINT('Ctrl Pts',(183.670064521709,-0.276524961665025,
339.912382847308));
#47098=CARTESIAN_POINT('Ctrl Pts',(183.662325297902,-0.139493633689289,
339.918178848906));
#47099=CARTESIAN_POINT('Ctrl Pts',(183.654586074095,-0.00253160902896628,
339.918249348443));
#47100=CARTESIAN_POINT('Ctrl Pts',(183.646838643908,0.134575644959302,339.918319922734));
#47101=CARTESIAN_POINT('Ctrl Pts',(183.639091213722,0.271613056281813,339.91265286719));
#47102=CARTESIAN_POINT('Ctrl Pts',(183.631343783536,0.408067137857272,339.901292102446));
#47103=CARTESIAN_POINT('Ctrl Pts',(183.623592233658,0.544593778820921,339.889925296621));
#47104=CARTESIAN_POINT('Ctrl Pts',(183.615840683779,0.680536083323476,339.872858797906));
#47105=CARTESIAN_POINT('Ctrl Pts',(183.608089133901,0.815388600765422,339.850188088337));
#47106=CARTESIAN_POINT('Ctrl Pts',(183.600325114227,0.950458053320495,339.827480908755));
#47107=CARTESIAN_POINT('Ctrl Pts',(183.592561094553,1.08443383191718,339.799151584073));
#47108=CARTESIAN_POINT('Ctrl Pts',(183.584797074879,1.21682267218757,339.765346330221));
#47109=CARTESIAN_POINT('Ctrl Pts',(183.577280918871,1.34498504412012,339.732620297509));
#47110=CARTESIAN_POINT('Ctrl Pts',(183.569764762863,1.47165996656069,339.694762775491));
#47111=CARTESIAN_POINT('Ctrl Pts',(183.562248606856,1.5964178399923,339.65194939167));
#47112=CARTESIAN_POINT('Ctrl Pts',(183.554470990015,1.72551560439166,339.607646679658));
#47113=CARTESIAN_POINT('Ctrl Pts',(183.546693373173,1.8529707700418,339.557896287814));
#47114=CARTESIAN_POINT('Ctrl Pts',(183.538915756332,1.97828959446425,339.50283836518));
#47115=CARTESIAN_POINT('Ctrl Pts',(183.531147691353,2.10345451208518,339.44784806039));
#47116=CARTESIAN_POINT('Ctrl Pts',(183.523379626374,2.22648795474663,339.387563350159));
#47117=CARTESIAN_POINT('Ctrl Pts',(183.515611561395,2.34691190214015,339.322173942138));
#47118=CARTESIAN_POINT('Ctrl Pts',(183.507851182931,2.46721668979935,339.256849237065));
#47119=CARTESIAN_POINT('Ctrl Pts',(183.500090804468,2.58491677974573,339.186430071531));
#47120=CARTESIAN_POINT('Ctrl Pts',(183.492330426004,2.69955501941842,339.111153823397));
#47121=CARTESIAN_POINT('Ctrl Pts',(183.484575875352,2.81410716921139,339.035934105468));
#47122=CARTESIAN_POINT('Ctrl Pts',(183.4768213247,2.92560172037708,338.955864778789));
#47123=CARTESIAN_POINT('Ctrl Pts',(183.469066774049,3.03360730182606,338.871228461459));
#47124=CARTESIAN_POINT('Ctrl Pts',(183.461315500151,3.14156724454938,338.786627907962));
#47125=CARTESIAN_POINT('Ctrl Pts',(183.453564226254,3.24604084307936,338.697464442576));
#47126=CARTESIAN_POINT('Ctrl Pts',(183.445812952357,3.3466270258048,338.604063070016));
#47127=CARTESIAN_POINT('Ctrl Pts',(183.438063287257,3.44719233160352,338.510681083157));
#47128=CARTESIAN_POINT('Ctrl Pts',(183.430313622157,3.5438715404598,338.413063204326));
#47129=CARTESIAN_POINT('Ctrl Pts',(183.422563957057,3.63629821021753,338.311573400797));
#47130=CARTESIAN_POINT('Ctrl Pts',(183.414814226142,3.72872566493115,338.210082735342));
#47131=CARTESIAN_POINT('Ctrl Pts',(183.407064495226,3.81690024553004,338.104720368382));
#47132=CARTESIAN_POINT('Ctrl Pts',(183.39931476431,3.90049407107727,337.995885355615));
#47133=CARTESIAN_POINT('Ctrl Pts',(183.39156329328,3.98410666667491,337.887025905175));
#47134=CARTESIAN_POINT('Ctrl Pts',(183.383811822249,4.06313622261014,337.774692567));
#47135=CARTESIAN_POINT('Ctrl Pts',(183.376060351219,4.13729690671077,337.659315206632));
#47136=CARTESIAN_POINT('Ctrl Pts',(183.368300672718,4.21153611418,337.543815681546));
#47137=CARTESIAN_POINT('Ctrl Pts',(183.360540994217,4.28089594008427,337.425266024898));
#47138=CARTESIAN_POINT('Ctrl Pts',(183.352781315717,4.34513517033009,337.304123133442));
#47139=CARTESIAN_POINT('Ctrl Pts',(183.345017497428,4.40940867220259,337.182915612258));
#47140=CARTESIAN_POINT('Ctrl Pts',(183.337253679139,4.46855596658702,337.059112451734));
#47141=CARTESIAN_POINT('Ctrl Pts',(183.32948986085,4.52238355654552,336.933191669232));
#47142=CARTESIAN_POINT('Ctrl Pts',(183.321713662257,4.57629698080395,336.80707009152));
#47143=CARTESIAN_POINT('Ctrl Pts',(183.313937463665,4.62487361085573,336.678824509432));
#47144=CARTESIAN_POINT('Ctrl Pts',(183.306161265072,4.66796921373637,336.548950122538));
#47145=CARTESIAN_POINT('Ctrl Pts',(183.298777700908,4.7088888411416,336.425633329966));
#47146=CARTESIAN_POINT('Ctrl Pts',(183.291394136745,4.74486729916818,336.300848455172));
#47147=CARTESIAN_POINT('Ctrl Pts',(183.284010572581,4.77582394746742,336.175027099814));
#47148=CARTESIAN_POINT('Ctrl Pts',(183.276234394037,4.8084266876837,336.042515307105));
#47149=CARTESIAN_POINT('Ctrl Pts',(183.268458215494,4.83556150200425,335.90843692987));
#47150=CARTESIAN_POINT('Ctrl Pts',(183.26068203695,4.85707903122376,335.773282837613));
#47151=CARTESIAN_POINT('Ctrl Pts',(183.252915403468,4.87857014822109,335.638294643581));
#47152=CARTESIAN_POINT('Ctrl Pts',(183.245148769986,4.8944576385936,335.502233744006));
#47153=CARTESIAN_POINT('Ctrl Pts',(183.237382136505,4.90464232427141,335.365604613573));
#47154=CARTESIAN_POINT('Ctrl Pts',(183.229623181197,4.91481694126381,335.229110556108));
#47155=CARTESIAN_POINT('Ctrl Pts',(183.22186422589,4.91929994442945,335.092049772895));
#47156=CARTESIAN_POINT('Ctrl Pts',(183.214105270582,4.91804353454062,334.954934992919));
#47157=CARTESIAN_POINT('Ctrl Pts',(183.206352133207,4.91678806675131,334.81792302634));
#47158=CARTESIAN_POINT('Ctrl Pts',(183.198598995832,4.90980175566383,334.680857532755));
#47159=CARTESIAN_POINT('Ctrl Pts',(183.190845858457,4.89708879725493,334.544254046315));
#47160=CARTESIAN_POINT('Ctrl Pts',(183.183095977539,4.88438117851743,334.407707935799));
#47161=CARTESIAN_POINT('Ctrl Pts',(183.175346096622,4.86595173250282,334.271623834738));
#47162=CARTESIAN_POINT('Ctrl Pts',(183.167596215704,4.84185669610816,334.136514738486));
#47163=CARTESIAN_POINT('Ctrl Pts',(183.159847930984,4.81776662242882,334.001433469873));
#47164=CARTESIAN_POINT('Ctrl Pts',(183.152099646265,4.78801334800257,333.867327191067));
#47165=CARTESIAN_POINT('Ctrl Pts',(183.144351361545,4.7527046142189,333.734700860475));
#47166=CARTESIAN_POINT('Ctrl Pts',(183.136602997014,4.71739551673801,333.602073163767));
#47167=CARTESIAN_POINT('Ctrl Pts',(183.128854632484,4.67653094633414,333.470925823261));
#47168=CARTESIAN_POINT('Ctrl Pts',(183.121106267953,4.63026901798813,333.341750355477));
#47169=CARTESIAN_POINT('Ctrl Pts',(183.113356147906,4.58399660826075,333.212545620921));
#47170=CARTESIAN_POINT('Ctrl Pts',(183.105606027859,4.5323245389347,333.085314015891));
#47171=CARTESIAN_POINT('Ctrl Pts',(183.097855907812,4.47545958671199,332.960528364942));
#47172=CARTESIAN_POINT('Ctrl Pts',(183.090097548043,4.41853417717562,332.835610045188));
#47173=CARTESIAN_POINT('Ctrl Pts',(183.082339188273,4.35640501844851,332.713143230329));
#47174=CARTESIAN_POINT('Ctrl Pts',(183.074580828504,4.28932576175322,332.593577848327));
#47175=CARTESIAN_POINT('Ctrl Pts',(183.066818313455,4.22221057826133,332.473948428628));
#47176=CARTESIAN_POINT('Ctrl Pts',(183.059055798407,4.15014021918361,332.357223870529));
#47177=CARTESIAN_POINT('Ctrl Pts',(183.051293283358,4.07341191337439,332.243825396228));
#47178=CARTESIAN_POINT('Ctrl Pts',(183.043518348122,3.99656084065466,332.130245481971));
#47179=CARTESIAN_POINT('Ctrl Pts',(183.035743412885,3.91503716072815,332.020002600387));
#47180=CARTESIAN_POINT('Ctrl Pts',(183.027968477649,3.82917920583801,331.913485838024));
#47181=CARTESIAN_POINT('Ctrl Pts',(183.020569831202,3.74747657635232,331.812124239317));
#47182=CARTESIAN_POINT('Ctrl Pts',(183.013171184755,3.66184956223402,331.714136757172));
#47183=CARTESIAN_POINT('Ctrl Pts',(183.005772538308,3.57261956977787,331.619826561826));
#47184=CARTESIAN_POINT('Ctrl Pts',(182.997998800428,3.47886585721643,331.52073509378));
#47185=CARTESIAN_POINT('Ctrl Pts',(182.990225062549,3.38083770587482,331.425390039951));
#47186=CARTESIAN_POINT('Ctrl Pts',(182.982451324669,3.27886659433371,331.334182639702));
#47187=CARTESIAN_POINT('Ctrl Pts',(182.974687171874,3.17702121403236,331.243087698946));
#47188=CARTESIAN_POINT('Ctrl Pts',(182.966923019079,3.07124283549676,331.156120519001));
#47189=CARTESIAN_POINT('Ctrl Pts',(182.959158866284,2.96190156216339,331.07363753602));
#47190=CARTESIAN_POINT('Ctrl Pts',(182.951402428827,2.85266894266215,330.991236517441));
#47191=CARTESIAN_POINT('Ctrl Pts',(182.94364599137,2.73988078423507,330.913311062166));
#47192=CARTESIAN_POINT('Ctrl Pts',(182.935889553914,2.62394196427249,330.840178894396));
#47193=CARTESIAN_POINT('Ctrl Pts',(182.928138968751,2.50809062107366,330.767101905429));
#47194=CARTESIAN_POINT('Ctrl Pts',(182.920388383589,2.38909367739034,330.698811213191));
#47195=CARTESIAN_POINT('Ctrl Pts',(182.912637798426,2.26738653550387,330.635582357162));
#47196=CARTESIAN_POINT('Ctrl Pts',(182.904890513095,2.145731210755,330.572380420986));
#47197=CARTESIAN_POINT('Ctrl Pts',(182.897143227765,2.02136832905076,330.514236214586));
#47198=CARTESIAN_POINT('Ctrl Pts',(182.889395942434,1.89475934510586,330.461380156189));
#47199=CARTESIAN_POINT('Ctrl Pts',(182.881650279359,1.76817687265904,330.408535165675));
#47200=CARTESIAN_POINT('Ctrl Pts',(182.873904616285,1.63934959409558,330.360976271191));
#47201=CARTESIAN_POINT('Ctrl Pts',(182.86615895321,1.50876010339829,330.318886242261));
#47202=CARTESIAN_POINT('Ctrl Pts',(182.858413233964,1.37816966568314,330.2767959081));
#47203=CARTESIAN_POINT('Ctrl Pts',(182.850667514719,1.24581736251209,330.24017463858));
#47204=CARTESIAN_POINT('Ctrl Pts',(182.842921795473,1.11220176748111,330.209155576424));
#47205=CARTESIAN_POINT('Ctrl Pts',(182.83517434195,0.978556255715918,330.178129569052));
#47206=CARTESIAN_POINT('Ctrl Pts',(182.827426888426,0.843647270077547,330.152708353432));
#47207=CARTESIAN_POINT('Ctrl Pts',(182.819679434902,0.707984019387355,330.132974040465));
#47208=CARTESIAN_POINT('Ctrl Pts',(182.811923760379,0.572176813319829,330.113218786966));
#47209=CARTESIAN_POINT('Ctrl Pts',(182.804168085855,0.435614130961163,330.099162546979));
#47210=CARTESIAN_POINT('Ctrl Pts',(182.796412411331,0.298811309764709,330.090835624706));
#47211=CARTESIAN_POINT('Ctrl Pts',(182.788652595967,0.161935448033445,330.082504256597));
#47212=CARTESIAN_POINT('Ctrl Pts',(182.780892780603,0.0248195827529,330.079908308776));
#47213=CARTESIAN_POINT('Ctrl Pts',(182.773132965239,-0.112021492345339,
330.08302590532));
#47214=CARTESIAN_POINT('Ctrl Pts',(182.765360727264,-0.249081634955755,
330.086148492794));
#47215=CARTESIAN_POINT('Ctrl Pts',(182.75758848929,-0.385865717896615,330.095002877277));
#47216=CARTESIAN_POINT('Ctrl Pts',(182.749816251315,-0.521863715696806,
330.109515225999));
#47217=CARTESIAN_POINT('Ctrl Pts',(182.742389002221,-0.651825125676095,
330.123383410329));
#47218=CARTESIAN_POINT('Ctrl Pts',(182.734961753127,-0.781068451306207,
330.142417990637));
#47219=CARTESIAN_POINT('Ctrl Pts',(182.727534504033,-0.909159619807499,
330.166511420494));
#47220=CARTESIAN_POINT('Ctrl Pts',(182.719758964722,-1.04325744035854,330.191734677267));
#47221=CARTESIAN_POINT('Ctrl Pts',(182.71198342541,-1.17651648894425,330.222582492355));
#47222=CARTESIAN_POINT('Ctrl Pts',(182.704207886098,-1.30842819381469,330.258987584478));
#47223=CARTESIAN_POINT('Ctrl Pts',(182.696441910889,-1.44017764408495,330.295347897455));
#47224=CARTESIAN_POINT('Ctrl Pts',(182.688675935679,-1.5705826749916,330.337251783594));
#47225=CARTESIAN_POINT('Ctrl Pts',(182.68090996047,-1.69914310592826,330.384580650897));
#47226=CARTESIAN_POINT('Ctrl Pts',(182.67315168168,-1.82757612788094,330.431862613232));
#47227=CARTESIAN_POINT('Ctrl Pts',(182.665393402889,-1.95416782345623,330.484558723225));
#47228=CARTESIAN_POINT('Ctrl Pts',(182.657635124099,-2.07843177080675,330.54250020341));
#47229=CARTESIAN_POINT('Ctrl Pts',(182.649882680715,-2.20260225277733,330.600398102793));
#47230=CARTESIAN_POINT('Ctrl Pts',(182.64213023733,-2.32444811867142,330.663533354894));
#47231=CARTESIAN_POINT('Ctrl Pts',(182.634377793945,-2.4435019217258,330.731688692115));
#47232=CARTESIAN_POINT('Ctrl Pts',(182.62662863126,-2.56250534327389,330.799815187178));
#47233=CARTESIAN_POINT('Ctrl Pts',(182.618879468574,-2.6787187135427,330.872957348278));
#47234=CARTESIAN_POINT('Ctrl Pts',(182.611130305889,-2.79169844638803,330.95085158991));
#47235=CARTESIAN_POINT('Ctrl Pts',(182.603382754074,-2.90465469338577,331.028729639148));
#47236=CARTESIAN_POINT('Ctrl Pts',(182.595635202259,-3.01437831845557,331.111357582315));
#47237=CARTESIAN_POINT('Ctrl Pts',(182.587887650443,-3.12045437792336,331.198428280593));
#47238=CARTESIAN_POINT('Ctrl Pts',(182.580140032842,-3.22653133810722,331.285499718207));
#47239=CARTESIAN_POINT('Ctrl Pts',(182.572392415241,-3.32896036882893,331.37701373821));
#47240=CARTESIAN_POINT('Ctrl Pts',(182.564644797639,-3.42735962124693,331.472622916508));
#47241=CARTESIAN_POINT('Ctrl Pts',(182.556895437908,-3.52578099972094,331.568253593485));
#47242=CARTESIAN_POINT('Ctrl Pts',(182.549146078177,-3.62017051653461,331.667980988829));
#47243=CARTESIAN_POINT('Ctrl Pts',(182.541396718447,-3.71018348837263,331.771421126082));
#47244=CARTESIAN_POINT('Ctrl Pts',(182.533639136018,-3.80029197125682,331.874971021691));
#47245=CARTESIAN_POINT('Ctrl Pts',(182.52588155359,-3.88601437564062,331.982241233484));
#47246=CARTESIAN_POINT('Ctrl Pts',(182.518123971161,-3.96704627203496,332.092814602053));
#47247=CARTESIAN_POINT('Ctrl Pts',(182.51036224395,-4.04812146279008,332.203447048635));
#47248=CARTESIAN_POINT('Ctrl Pts',(182.50260051674,-4.12450093443874,332.317385844135));
#47249=CARTESIAN_POINT('Ctrl Pts',(182.494838789529,-4.19592443337213,332.434186052745));
#47250=CARTESIAN_POINT('Ctrl Pts',(182.487064652255,-4.26746212983944,332.551173010757));
#47251=CARTESIAN_POINT('Ctrl Pts',(182.479290514981,-4.33402782923239,332.671030182347));
#47252=CARTESIAN_POINT('Ctrl Pts',(182.471516377708,-4.39540755167253,332.793288528783));
#47253=CARTESIAN_POINT('Ctrl Pts',(182.464109741725,-4.45388571392279,332.909767442912));
#47254=CARTESIAN_POINT('Ctrl Pts',(182.456703105742,-4.50765687201246,333.028425445668));
#47255=CARTESIAN_POINT('Ctrl Pts',(182.449296469759,-4.55657774852652,333.148842987715));
#47256=CARTESIAN_POINT('Ctrl Pts',(182.440339878659,-4.61573608818309,333.294459795111));
#47257=CARTESIAN_POINT('Ctrl Pts',(182.431383287559,-4.6679636105574,333.44304691552));
#47258=CARTESIAN_POINT('Ctrl Pts',(182.42242669646,-4.7129878843127,333.59396718928));
#47259=CARTESIAN_POINT('Ctrl Pts',(182.413727250667,-4.75671950324406,333.740554515417));
#47260=CARTESIAN_POINT('Ctrl Pts',(182.405027804873,-4.79365563198517,333.889342650309));
#47261=CARTESIAN_POINT('Ctrl Pts',(182.39632835908,-4.82359349480214,334.0397245919));
#47262=CARTESIAN_POINT('Ctrl Pts',(182.387243195327,-4.8548587492319,334.196774201427));
#47263=CARTESIAN_POINT('Ctrl Pts',(182.378158031574,-4.87849083595186,334.355562030965));
#47264=CARTESIAN_POINT('Ctrl Pts',(182.36907286782,-4.89431507868469,334.515373367364));
#47265=CARTESIAN_POINT('Ctrl Pts',(182.360444744031,-4.90934326407371,334.667145204489));
#47266=CARTESIAN_POINT('Ctrl Pts',(182.351816620241,-4.91732970925359,334.819839802589));
#47267=CARTESIAN_POINT('Ctrl Pts',(182.343188496452,-4.91817494046866,334.972828002537));
#47268=CARTESIAN_POINT('Ctrl Pts',(182.342731456488,-4.91821971317398,334.980931933712));
#47269=CARTESIAN_POINT('Ctrl Pts',(182.342274416524,-4.91824445986726,334.989036685278));
#47270=CARTESIAN_POINT('Ctrl Pts',(182.34181737656,-4.91824916970108,334.997142162596));
#47271=CARTESIAN_POINT('',(180.591817376458,-4.9182484086652,335.003956407744));
#47272=CARTESIAN_POINT('Ctrl Pts',(182.341817376508,-4.91824916970162,334.997142163525));
#47273=CARTESIAN_POINT('Ctrl Pts',(182.33399174791,-4.91832981341144,335.135927521746));
#47274=CARTESIAN_POINT('Ctrl Pts',(182.326166119313,-4.91253165524224,335.274724294722));
#47275=CARTESIAN_POINT('Ctrl Pts',(182.318340490715,-4.9008783981803,335.413006039604));
#47276=CARTESIAN_POINT('Ctrl Pts',(182.310513578694,-4.88922322995347,335.551310463057));
#47277=CARTESIAN_POINT('Ctrl Pts',(182.302686666673,-4.87171108188477,335.689099311701));
#47278=CARTESIAN_POINT('Ctrl Pts',(182.294859754651,-4.84841756392563,335.825851190177));
#47279=CARTESIAN_POINT('Ctrl Pts',(182.287029996697,-4.82511557624064,335.962652792827));
#47280=CARTESIAN_POINT('Ctrl Pts',(182.279200238742,-4.79602809592471,336.098416300174));
#47281=CARTESIAN_POINT('Ctrl Pts',(182.271370480788,-4.76128183031932,336.232630680606));
#47282=CARTESIAN_POINT('Ctrl Pts',(182.263536312831,-4.72651599436453,336.366920655415));
#47283=CARTESIAN_POINT('Ctrl Pts',(182.255702144874,-4.68608512077128,336.499659398574));
#47284=CARTESIAN_POINT('Ctrl Pts',(182.247867976918,-4.64016564754835,336.630351442423));
#47285=CARTESIAN_POINT('Ctrl Pts',(182.240023128865,-4.59418357362901,336.761221654975));
#47286=CARTESIAN_POINT('Ctrl Pts',(182.232178280813,-4.54269808447251,336.890039238294));
#47287=CARTESIAN_POINT('Ctrl Pts',(182.224333432761,-4.48593385809718,337.016328466118));
#47288=CARTESIAN_POINT('Ctrl Pts',(182.216482296267,-4.42912412943677,337.142718927568));
#47289=CARTESIAN_POINT('Ctrl Pts',(182.208631159773,-4.36702740073226,337.26657665641));
#47290=CARTESIAN_POINT('Ctrl Pts',(182.20078002328,-4.29991371734091,337.387451588184));
#47291=CARTESIAN_POINT('Ctrl Pts',(182.192916621086,-4.23269518335661,337.508515360857));
#47292=CARTESIAN_POINT('Ctrl Pts',(182.185053218892,-4.16044424171952,337.626586709176));
#47293=CARTESIAN_POINT('Ctrl Pts',(182.177189816698,-4.08347386544473,337.741245018733));
#47294=CARTESIAN_POINT('Ctrl Pts',(182.175146022961,-4.06346832978651,337.771046106001));
#47295=CARTESIAN_POINT('Ctrl Pts',(182.173102229223,-4.04314418357207,337.800616806267));
#47296=CARTESIAN_POINT('Ctrl Pts',(182.171058435486,-4.02250734998357,337.829950120025));
#47297=CARTESIAN_POINT('Ctrl Pts',(182.16328355021,-3.94400186741796,337.941538263717));
#47298=CARTESIAN_POINT('Ctrl Pts',(182.155508664934,-3.86072540937495,338.050033628111));
#47299=CARTESIAN_POINT('Ctrl Pts',(182.147733779658,-3.77294980454117,338.155001241666));
#47300=CARTESIAN_POINT('Ctrl Pts',(182.139968464733,-3.68528224545914,338.259839647285));
#47301=CARTESIAN_POINT('Ctrl Pts',(182.132203149808,-3.59312680724248,338.361158645223));
#47302=CARTESIAN_POINT('Ctrl Pts',(182.124437834883,-3.49679854697354,338.458552151462));
#47303=CARTESIAN_POINT('Ctrl Pts',(182.116680221882,-3.4005658286088,338.555849059247));
#47304=CARTESIAN_POINT('Ctrl Pts',(182.108922608881,-3.3001687976538,338.649227947372));
#47305=CARTESIAN_POINT('Ctrl Pts',(182.10116499588,-3.19596249181755,338.738316039796));
#47306=CARTESIAN_POINT('Ctrl Pts',(182.093413223056,-3.09183463578897,338.827337063882));
#47307=CARTESIAN_POINT('Ctrl Pts',(182.085661450232,-2.98390350889375,338.91207346892));
#47308=CARTESIAN_POINT('Ctrl Pts',(182.077909677408,-2.87256042528724,338.992189833359));
#47309=CARTESIAN_POINT('Ctrl Pts',(182.070161190157,-2.76126453421413,339.072272240644));
#47310=CARTESIAN_POINT('Ctrl Pts',(182.062412702906,-2.64655987935621,339.147738274209));
#47311=CARTESIAN_POINT('Ctrl Pts',(182.054664215654,-2.52887004977796,339.218293414858));
#47312=CARTESIAN_POINT('Ctrl Pts',(182.046917342142,-2.41120473087652,339.288833861338));
#47313=CARTESIAN_POINT('Ctrl Pts',(182.03917046863,-2.29055580892797,339.354465248391));
#47314=CARTESIAN_POINT('Ctrl Pts',(182.031423595117,-2.16737465034927,339.414937166883));
#47315=CARTESIAN_POINT('Ctrl Pts',(182.023676658045,-2.0441924811235,339.475409581521));
#47316=CARTESIAN_POINT('Ctrl Pts',(182.015929720973,-1.91847838472056,339.530722270901));
#47317=CARTESIAN_POINT('Ctrl Pts',(182.008182783901,-1.79070668527723,339.58067163523));
#47318=CARTESIAN_POINT('Ctrl Pts',(182.000434106285,-1.66290627871049,339.63063222194));
#47319=CARTESIAN_POINT('Ctrl Pts',(181.992685428669,-1.53304771319022,339.67522694348));
#47320=CARTESIAN_POINT('Ctrl Pts',(181.984936751053,-1.40162318581535,339.714301168517));
#47321=CARTESIAN_POINT('Ctrl Pts',(181.977179849391,-1.27005917124119,339.753416864917));
#47322=CARTESIAN_POINT('Ctrl Pts',(181.969422947729,-1.136926250029,339.787000248999));
#47323=CARTESIAN_POINT('Ctrl Pts',(181.961666046067,-1.0027301456108,339.814947073186));
#47324=CARTESIAN_POINT('Ctrl Pts',(181.953904999964,-0.868462341452754,
339.842908829103));
#47325=CARTESIAN_POINT('Ctrl Pts',(181.946143953861,-0.73313060769247,339.865227960748));
#47326=CARTESIAN_POINT('Ctrl Pts',(181.938382907758,-0.597247647113583,
339.881851934514));
#47327=CARTESIAN_POINT('Ctrl Pts',(181.930609445289,-0.461147296686841,
339.898502503838));
#47328=CARTESIAN_POINT('Ctrl Pts',(181.92283598282,-0.324494347060001,339.909439677019));
#47329=CARTESIAN_POINT('Ctrl Pts',(181.91506252035,-0.187804267934973,339.914663021962));
#47330=CARTESIAN_POINT('Ctrl Pts',(181.907648480638,-0.0574343486144119,
339.919644854318));
#47331=CARTESIAN_POINT('Ctrl Pts',(181.900234440925,0.0729690550090576,
339.919429431031));
#47332=CARTESIAN_POINT('Ctrl Pts',(181.892820401212,0.202963363140059,339.9140603309));
#47333=CARTESIAN_POINT('Ctrl Pts',(181.885045243003,0.339289354247273,339.908429715935));
#47334=CARTESIAN_POINT('Ctrl Pts',(181.877270084795,0.475596244312727,339.897112967862));
#47335=CARTESIAN_POINT('Ctrl Pts',(181.869494926586,0.611371120462187,339.880103320173));
#47336=CARTESIAN_POINT('Ctrl Pts',(181.861729335389,0.746978931217701,339.863114602155));
#47337=CARTESIAN_POINT('Ctrl Pts',(181.853963744193,0.882055646439472,339.84044697035));
#47338=CARTESIAN_POINT('Ctrl Pts',(181.846198152996,1.01608925616967,339.812145642642));
#47339=CARTESIAN_POINT('Ctrl Pts',(181.838440260699,1.1499899833858,339.783872373206));
#47340=CARTESIAN_POINT('Ctrl Pts',(181.830682368401,1.2828492831529,339.749976603193));
#47341=CARTESIAN_POINT('Ctrl Pts',(181.822924476104,1.41416152279385,339.71055519551));
#47342=CARTESIAN_POINT('Ctrl Pts',(181.815172421267,1.54537495595415,339.671163450642));
#47343=CARTESIAN_POINT('Ctrl Pts',(181.807420366431,1.67504327320611,339.626254455923));
#47344=CARTESIAN_POINT('Ctrl Pts',(181.799668311594,1.80267262601678,339.575975793851));
#47345=CARTESIAN_POINT('Ctrl Pts',(181.791919539193,1.93024793700624,339.525718421164));
#47346=CARTESIAN_POINT('Ctrl Pts',(181.784170766793,2.05578563779871,339.470096046254));
#47347=CARTESIAN_POINT('Ctrl Pts',(181.776421994392,2.17880881230689,339.409305526034));
#47348=CARTESIAN_POINT('Ctrl Pts',(181.768674833861,2.30180639601633,339.34852765122));
#47349=CARTESIAN_POINT('Ctrl Pts',(181.760927673329,2.42229014365104,339.282583942509));
#47350=CARTESIAN_POINT('Ctrl Pts',(181.753180512798,2.53980520256777,339.211718484836));
#47351=CARTESIAN_POINT('Ctrl Pts',(181.745433287105,2.65732124989162,339.140852431121));
#47352=CARTESIAN_POINT('Ctrl Pts',(181.737686061413,2.7718682239794,339.065064747722));
#47353=CARTESIAN_POINT('Ctrl Pts',(181.729938835721,2.8830182131899,338.984644155369));
#47354=CARTESIAN_POINT('Ctrl Pts',(181.722189868152,2.99419319323221,338.904205481345));
#47355=CARTESIAN_POINT('Ctrl Pts',(181.714440900583,3.10196935196417,338.819132054661));
#47356=CARTESIAN_POINT('Ctrl Pts',(181.706691933014,3.20595028557887,338.729754124456));
#47357=CARTESIAN_POINT('Ctrl Pts',(181.698934740921,3.31004158147358,338.640281331166));
#47358=CARTESIAN_POINT('Ctrl Pts',(181.691177548827,3.41032930878365,338.546495163191));
#47359=CARTESIAN_POINT('Ctrl Pts',(181.683420356734,3.50645211354861,338.448764508906));
#47360=CARTESIAN_POINT('Ctrl Pts',(181.675659019479,3.60262628283465,338.350981630924));
#47361=CARTESIAN_POINT('Ctrl Pts',(181.667897682225,3.69463083285505,338.249250356418));
#47362=CARTESIAN_POINT('Ctrl Pts',(181.660136344971,3.78214412059007,338.143973427621));
#47363=CARTESIAN_POINT('Ctrl Pts',(181.652362593056,3.86979739036253,338.038528102922));
#47364=CARTESIAN_POINT('Ctrl Pts',(181.644588841141,3.95294480489276,337.929526101614));
#47365=CARTESIAN_POINT('Ctrl Pts',(181.636815089226,4.03130703749056,337.817400687155));
#47366=CARTESIAN_POINT('Ctrl Pts',(181.629404181797,4.10601166636027,337.710508792981));
#47367=CARTESIAN_POINT('Ctrl Pts',(181.621993274367,4.17636757725118,337.600778720445));
#47368=CARTESIAN_POINT('Ctrl Pts',(181.614582366938,4.24217217030331,337.488605701995));
#47369=CARTESIAN_POINT('Ctrl Pts',(181.606807279412,4.31121047303492,337.370920378725));
#47370=CARTESIAN_POINT('Ctrl Pts',(181.599032191885,4.37545695737443,337.250174054834));
#47371=CARTESIAN_POINT('Ctrl Pts',(181.591257104359,4.43462836544519,337.1267943772));
#47372=CARTESIAN_POINT('Ctrl Pts',(181.583491584237,4.49372696188098,337.003566520797));
#47373=CARTESIAN_POINT('Ctrl Pts',(181.575726064116,4.54776274037067,336.877712107178));
#47374=CARTESIAN_POINT('Ctrl Pts',(181.567960543995,4.59649664601165,336.749686156345));
#47375=CARTESIAN_POINT('Ctrl Pts',(181.560202723087,4.64518223386508,336.621787138303));
#47376=CARTESIAN_POINT('Ctrl Pts',(181.552444902179,4.68857627164759,336.491721230579));
#47377=CARTESIAN_POINT('Ctrl Pts',(181.544687081272,4.72648658466573,336.359966039089));
#47378=CARTESIAN_POINT('Ctrl Pts',(181.536935098061,4.76436837048295,336.228309992304));
#47379=CARTESIAN_POINT('Ctrl Pts',(181.52918311485,4.79677453740265,336.094967566079));
#47380=CARTESIAN_POINT('Ctrl Pts',(181.521431131639,4.82356193879182,335.960433904618));
#47381=CARTESIAN_POINT('Ctrl Pts',(181.513682430966,4.85033799719381,335.825957210742));
#47382=CARTESIAN_POINT('Ctrl Pts',(181.505933730292,4.87149994602879,335.690290667441));
#47383=CARTESIAN_POINT('Ctrl Pts',(181.498185029619,4.88695523757201,335.553941845745));
#47384=CARTESIAN_POINT('Ctrl Pts',(181.490437940866,4.90240731403442,335.417621387958));
#47385=CARTESIAN_POINT('Ctrl Pts',(181.482690852113,4.91215505048446,335.280619322229));
#47386=CARTESIAN_POINT('Ctrl Pts',(181.47494376336,4.91615755399456,335.143450224128));
#47387=CARTESIAN_POINT('Ctrl Pts',(181.467196609428,4.92016009117888,335.006279971982));
#47388=CARTESIAN_POINT('Ctrl Pts',(181.459449455496,4.91841728761306,334.868943075368));
#47389=CARTESIAN_POINT('Ctrl Pts',(181.451702301565,4.9109403648797,334.731955609842));
#47390=CARTESIAN_POINT('Ctrl Pts',(181.443953405669,4.90346176094433,334.594937342392));
#47391=CARTESIAN_POINT('Ctrl Pts',(181.436204509773,4.89024649351901,334.458269052591));
#47392=CARTESIAN_POINT('Ctrl Pts',(181.428455613878,4.87135775702261,334.32246279394));
#47393=CARTESIAN_POINT('Ctrl Pts',(181.420698492911,4.85244897106461,334.186512383647));
#47394=CARTESIAN_POINT('Ctrl Pts',(181.412941371945,4.82785474024287,334.051426220067));
#47395=CARTESIAN_POINT('Ctrl Pts',(181.405184250979,4.79768971904116,333.91770779255));
#47396=CARTESIAN_POINT('Ctrl Pts',(181.397422984667,4.76750857788533,333.783917906939));
#47397=CARTESIAN_POINT('Ctrl Pts',(181.389661718355,4.73175081628115,333.651497590957));
#47398=CARTESIAN_POINT('Ctrl Pts',(181.381900452044,4.69058104699797,333.520935260361));
#47399=CARTESIAN_POINT('Ctrl Pts',(181.374126770034,4.64934541843374,333.390164069202));
#47400=CARTESIAN_POINT('Ctrl Pts',(181.366353088024,4.60268061488252,333.261257170529));
#47401=CARTESIAN_POINT('Ctrl Pts',(181.358579406015,4.55079981485308,333.134683912139));
#47402=CARTESIAN_POINT('Ctrl Pts',(181.351167714898,4.50133490694478,333.014004690416));
#47403=CARTESIAN_POINT('Ctrl Pts',(181.343756023781,4.44712896206334,332.895446927018));
#47404=CARTESIAN_POINT('Ctrl Pts',(181.336344332664,4.3884047778019,332.779394999405));
#47405=CARTESIAN_POINT('Ctrl Pts',(181.328569281178,4.32680162287936,332.657653591403));
#47406=CARTESIAN_POINT('Ctrl Pts',(181.320794229692,4.26003132370039,332.538285192771));
#47407=CARTESIAN_POINT('Ctrl Pts',(181.313019178206,4.18830020322877,332.421759423534));
#47408=CARTESIAN_POINT('Ctrl Pts',(181.305253694836,4.11665735634828,332.30537705298));
#47409=CARTESIAN_POINT('Ctrl Pts',(181.297488211466,4.0400660380698,332.191830681109));
#47410=CARTESIAN_POINT('Ctrl Pts',(181.289722728097,3.95877951105733,332.081567570538));
#47411=CARTESIAN_POINT('Ctrl Pts',(181.281964944609,3.8775735838805,331.971413791599));
#47412=CARTESIAN_POINT('Ctrl Pts',(181.274207161122,3.79168194321293,331.864537107879));
#47413=CARTESIAN_POINT('Ctrl Pts',(181.266449377634,3.70140221459444,331.761357582521));
#47414=CARTESIAN_POINT('Ctrl Pts',(181.25869743247,3.61119042835433,331.658255707621));
#47415=CARTESIAN_POINT('Ctrl Pts',(181.250945487307,3.51659738372394,331.55884574585));
#47416=CARTESIAN_POINT('Ctrl Pts',(181.243193542143,3.41796198681423,331.463516023054));
#47417=CARTESIAN_POINT('Ctrl Pts',(181.235444880338,3.31936836721765,331.368226677444));
#47418=CARTESIAN_POINT('Ctrl Pts',(181.227696218533,3.21673608116487,331.277014404625));
#47419=CARTESIAN_POINT('Ctrl Pts',(181.219947556729,3.11044186705358,331.190231705972));
#47420=CARTESIAN_POINT('Ctrl Pts',(181.212200507339,3.00416977165798,331.103467065893));
#47421=CARTESIAN_POINT('Ctrl Pts',(181.20445345795,2.89423756648427,331.021130413605));
#47422=CARTESIAN_POINT('Ctrl Pts',(181.196706408561,2.78105583393632,330.943534603743));
#47423=CARTESIAN_POINT('Ctrl Pts',(181.188959294453,2.66787315586401,330.865938145643));
#47424=CARTESIAN_POINT('Ctrl Pts',(181.181212180345,2.5514412186582,330.79308282999));
#47425=CARTESIAN_POINT('Ctrl Pts',(181.173465066236,2.432200068598,330.725238499189));
#47426=CARTESIAN_POINT('Ctrl Pts',(181.165716210588,2.31293211329592,330.657378917079));
#47427=CARTESIAN_POINT('Ctrl Pts',(181.157967354939,2.19085402818108,330.594532754615));
#47428=CARTESIAN_POINT('Ctrl Pts',(181.150218499291,2.06643060311088,330.536923972749));
#47429=CARTESIAN_POINT('Ctrl Pts',(181.142461419019,1.94187511521186,330.479254045011));
#47430=CARTESIAN_POINT('Ctrl Pts',(181.134704338747,1.81496966992982,330.426832766878));
#47431=CARTESIAN_POINT('Ctrl Pts',(181.126947258475,1.68619970361795,330.379836190997));
#47432=CARTESIAN_POINT('Ctrl Pts',(181.119186033166,1.55736092838004,330.332814502243));
#47433=CARTESIAN_POINT('Ctrl Pts',(181.111424807856,1.42665601914718,330.291223410162));
#47434=CARTESIAN_POINT('Ctrl Pts',(181.103663582547,1.29458477212117,330.2551887993));
#47435=CARTESIAN_POINT('Ctrl Pts',(181.095889941655,1.16230225157505,330.219096544103));
#47436=CARTESIAN_POINT('Ctrl Pts',(181.088116300764,1.02864940678656,330.188578619371));
#47437=CARTESIAN_POINT('Ctrl Pts',(181.080342659872,0.894136281243819,330.163709750949));
#47438=CARTESIAN_POINT('Ctrl Pts',(181.072930539378,0.765878813670063,330.139997432376));
#47439=CARTESIAN_POINT('Ctrl Pts',(181.065518418884,0.636839567267541,330.121420597274));
#47440=CARTESIAN_POINT('Ctrl Pts',(181.05810629839,0.507462422473141,330.10799990267));
#47441=CARTESIAN_POINT('Ctrl Pts',(181.050331206421,0.371749680048379,330.09392199677));
#47442=CARTESIAN_POINT('Ctrl Pts',(181.042556114452,0.23523622890904,330.08547349236));
#47443=CARTESIAN_POINT('Ctrl Pts',(181.034781022483,0.0984286415098769,
330.082735021882));
#47444=CARTESIAN_POINT('Ctrl Pts',(181.027015498113,-0.0382105980329883,
330.079999921214));
#47445=CARTESIAN_POINT('Ctrl Pts',(181.019249973743,-0.175142866604414,
330.0829608816));
#47446=CARTESIAN_POINT('Ctrl Pts',(181.011484449372,-0.311854991428378,
330.091646963917));
#47447=CARTESIAN_POINT('Ctrl Pts',(181.003726624413,-0.448431568055069,
330.100324434103));
#47448=CARTESIAN_POINT('Ctrl Pts',(180.995968799453,-0.584788047729505,
330.114715705278));
#47449=CARTESIAN_POINT('Ctrl Pts',(180.988210974494,-0.720410123561506,
330.134797813413));
#47450=CARTESIAN_POINT('Ctrl Pts',(180.980458987433,-0.855930141424833,
330.154864809412));
#47451=CARTESIAN_POINT('Ctrl Pts',(180.972707000371,-0.990716470371876,
330.180614061333));
#47452=CARTESIAN_POINT('Ctrl Pts',(180.96495501331,-1.1242591532953,330.211970716596));
#47453=CARTESIAN_POINT('Ctrl Pts',(180.957206309108,-1.25774528273297,330.243314092749));
#47454=CARTESIAN_POINT('Ctrl Pts',(180.949457604907,-1.3899884339188,330.280260060053));
#47455=CARTESIAN_POINT('Ctrl Pts',(180.941708900705,-1.52048830249585,330.322682565351));
#47456=CARTESIAN_POINT('Ctrl Pts',(180.933961808621,-1.65096102058404,330.365096244649));
#47457=CARTESIAN_POINT('Ctrl Pts',(180.926214716537,-1.77969080598771,330.412984074842));
#47458=CARTESIAN_POINT('Ctrl Pts',(180.918467624452,-1.90619237957513,330.466170087603));
#47459=CARTESIAN_POINT('Ctrl Pts',(180.910720467391,-2.03269501417282,330.519356546452));
#47460=CARTESIAN_POINT('Ctrl Pts',(180.902973310329,-2.15696903935685,330.577841125011));
#47461=CARTESIAN_POINT('Ctrl Pts',(180.895226153267,-2.2785494015976,330.641399801888));
#47462=CARTESIAN_POINT('Ctrl Pts',(180.887477254447,-2.40015709820899,330.70497276838));
#47463=CARTESIAN_POINT('Ctrl Pts',(180.879728355626,-2.51906958046477,330.773621922178));
#47464=CARTESIAN_POINT('Ctrl Pts',(180.871979456806,-2.6348469875833,330.847077605526));
#47465=CARTESIAN_POINT('Ctrl Pts',(180.864222333259,-2.75074728151859,330.920611255166));
#47466=CARTESIAN_POINT('Ctrl Pts',(180.856465209712,-2.86350552257877,330.998961415703));
#47467=CARTESIAN_POINT('Ctrl Pts',(180.848708086165,-2.97271096425876,331.081815141488));
#47468=CARTESIAN_POINT('Ctrl Pts',(180.840946817456,-3.08197476188359,331.16471314169));
#47469=CARTESIAN_POINT('Ctrl Pts',(180.833185548747,-3.18768167610874,331.25211925348));
#47470=CARTESIAN_POINT('Ctrl Pts',(180.825424280037,-3.28945537701512,331.343681306953));
#47471=CARTESIAN_POINT('Ctrl Pts',(180.817650595971,-3.39139188080084,331.435389828185));
#47472=CARTESIAN_POINT('Ctrl Pts',(180.809876911904,-3.48938231888239,331.53126730242));
#47473=CARTESIAN_POINT('Ctrl Pts',(180.802103227837,-3.58308783646672,331.63092525778));
#47474=CARTESIAN_POINT('Ctrl Pts',(180.794691573263,-3.67242937929438,331.725942026445));
#47475=CARTESIAN_POINT('Ctrl Pts',(180.78727991869,-3.75787593256742,331.824394865921));
#47476=CARTESIAN_POINT('Ctrl Pts',(180.779868264116,-3.83916996566935,331.92592175812));
#47477=CARTESIAN_POINT('Ctrl Pts',(180.772032810466,-3.92511239891202,332.033253967166));
#47478=CARTESIAN_POINT('Ctrl Pts',(180.764197356815,-4.00669427622042,332.144372848535));
#47479=CARTESIAN_POINT('Ctrl Pts',(180.756361903165,-4.0835628426182,332.258887530055));
#47480=CARTESIAN_POINT('Ctrl Pts',(180.748614019154,-4.15957231994044,332.37212238659));
#47481=CARTESIAN_POINT('Ctrl Pts',(180.740866135143,-4.23097303984883,332.488677217721));
#47482=CARTESIAN_POINT('Ctrl Pts',(180.733118251132,-4.29746242262358,332.608138844197));
#47483=CARTESIAN_POINT('Ctrl Pts',(180.725377872357,-4.363887398328,332.727484750343));
#47484=CARTESIAN_POINT('Ctrl Pts',(180.717637493582,-4.42541031130816,332.849731510328));
#47485=CARTESIAN_POINT('Ctrl Pts',(180.709897114807,-4.48177151165708,332.974436577197));
#47486=CARTESIAN_POINT('Ctrl Pts',(180.702162542361,-4.53809043349586,333.099048098427));
#47487=CARTESIAN_POINT('Ctrl Pts',(180.694427969915,-4.58925518601485,333.226113901423));
#47488=CARTESIAN_POINT('Ctrl Pts',(180.68669339747,-4.6350519673576,333.355166779763));
#47489=CARTESIAN_POINT('Ctrl Pts',(180.678787062389,-4.68186576364981,333.487085551791));
#47490=CARTESIAN_POINT('Ctrl Pts',(180.670880727309,-4.72307016559635,333.621080326329));
#47491=CARTESIAN_POINT('Ctrl Pts',(180.662974392229,-4.75848864658392,333.756630037828));
#47492=CARTESIAN_POINT('Ctrl Pts',(180.655245615586,-4.79311170844795,333.889135608818));
#47493=CARTESIAN_POINT('Ctrl Pts',(180.647516838943,-4.82220588273384,334.023126615179));
#47494=CARTESIAN_POINT('Ctrl Pts',(180.639788062299,-4.84565678919855,334.158101345889));
#47495=CARTESIAN_POINT('Ctrl Pts',(180.631792948001,-4.86991582607383,334.297727375887));
#47496=CARTESIAN_POINT('Ctrl Pts',(180.623797833702,-4.88813555629895,334.438405718679));
#47497=CARTESIAN_POINT('Ctrl Pts',(180.615802719404,-4.9002471782909,334.579570869049));
#47498=CARTESIAN_POINT('Ctrl Pts',(180.607807605105,-4.91235880028286,334.720736019419));
#47499=CARTESIAN_POINT('Ctrl Pts',(180.599812490807,-4.91836229151515,334.862387513434));
#47500=CARTESIAN_POINT('Ctrl Pts',(180.591817376508,-4.9182484086659,335.003956406867));
#47501=CARTESIAN_POINT('',(178.84181737655,-4.91824988879026,335.001045903734));
#47502=CARTESIAN_POINT('Ctrl Pts',(180.591817376458,-4.9182484086652,335.003956407744));
#47503=CARTESIAN_POINT('Ctrl Pts',(180.582712087458,-4.91811871239747,335.165183081947));
#47504=CARTESIAN_POINT('Ctrl Pts',(180.573606798457,-4.9100573358069,335.326074667974));
#47505=CARTESIAN_POINT('Ctrl Pts',(180.564501509456,-4.894186142654,335.485927014637));
#47506=CARTESIAN_POINT('Ctrl Pts',(180.555336394497,-4.87821066842477,335.646829665117));
#47507=CARTESIAN_POINT('Ctrl Pts',(180.546171279538,-4.85432251810979,335.806679301925));
#47508=CARTESIAN_POINT('Ctrl Pts',(180.537006164579,-4.82269491367838,335.96477812583));
#47509=CARTESIAN_POINT('Ctrl Pts',(180.527773926185,-4.79083567511414,336.12403483332));
#47510=CARTESIAN_POINT('Ctrl Pts',(180.51854168779,-4.75112327297293,336.281514919373));
#47511=CARTESIAN_POINT('Ctrl Pts',(180.509309449396,-4.70378293552858,336.436526768957));
#47512=CARTESIAN_POINT('Ctrl Pts',(180.506749709545,-4.69065730519238,336.479505512777));
#47513=CARTESIAN_POINT('Ctrl Pts',(180.504189969693,-4.67694556728002,336.522294644668));
#47514=CARTESIAN_POINT('Ctrl Pts',(180.501630229842,-4.6626531617174,336.564879725738));
#47515=CARTESIAN_POINT('Ctrl Pts',(180.493855154817,-4.61924073233722,336.69422966732));
#47516=CARTESIAN_POINT('Ctrl Pts',(180.486080079792,-4.57037304221952,336.821976137904));
#47517=CARTESIAN_POINT('Ctrl Pts',(180.478305004767,-4.51618657349027,336.947624680457));
#47518=CARTESIAN_POINT('Ctrl Pts',(180.470539497528,-4.46206678508254,337.073118603501));
#47519=CARTESIAN_POINT('Ctrl Pts',(180.462773990289,-4.40264139431559,337.196519379768));
#47520=CARTESIAN_POINT('Ctrl Pts',(180.455008483049,-4.33809655530464,337.317347910728));
#47521=CARTESIAN_POINT('Ctrl Pts',(180.447250675388,-4.27361571314945,337.438056638986));
#47522=CARTESIAN_POINT('Ctrl Pts',(180.439492867727,-4.20402570722914,337.556197854845));
#47523=CARTESIAN_POINT('Ctrl Pts',(180.431735060066,-4.12956051163327,337.67131298115));
#47524=CARTESIAN_POINT('Ctrl Pts',(180.423983090452,-4.05515135394033,337.786341478926));
#47525=CARTESIAN_POINT('Ctrl Pts',(180.416231120837,-3.9758745205178,337.898348093026));
#47526=CARTESIAN_POINT('Ctrl Pts',(180.408479151223,-3.89200940936859,338.006899702332));
#47527=CARTESIAN_POINT('Ctrl Pts',(180.400730464632,-3.80817981579158,338.115405339129));
#47528=CARTESIAN_POINT('Ctrl Pts',(180.392981778041,-3.71976604779773,338.220458572709));
#47529=CARTESIAN_POINT('Ctrl Pts',(180.38523309145,-3.62709010415005,338.32165627946));
#47530=CARTESIAN_POINT('Ctrl Pts',(180.377486017074,-3.53443344293386,338.422832930717));
#47531=CARTESIAN_POINT('Ctrl Pts',(180.369738942698,-3.43751663379423,338.520155362682));
#47532=CARTESIAN_POINT('Ctrl Pts',(180.361991868321,-3.33670088054444,338.613254806442));
#47533=CARTESIAN_POINT('Ctrl Pts',(180.354244729049,-3.2358842827672,338.70635503009));
#47534=CARTESIAN_POINT('Ctrl Pts',(180.346497589776,-3.13116896289556,338.79523192979));
#47535=CARTESIAN_POINT('Ctrl Pts',(180.338750450503,-3.02295148050503,338.879555052968));
#47536=CARTESIAN_POINT('Ctrl Pts',(180.331001569535,-2.91470966889854,338.963897133486));
#47537=CARTESIAN_POINT('Ctrl Pts',(180.323252688567,-2.80296443630261,339.043683160093));
#47538=CARTESIAN_POINT('Ctrl Pts',(180.315503807599,-2.68814344063036,339.118624516158));
#47539=CARTESIAN_POINT('Ctrl Pts',(180.307746701906,-2.57320057301128,339.193645415593));
#47540=CARTESIAN_POINT('Ctrl Pts',(180.299989596212,-2.45517574873292,339.263811158537));
#47541=CARTESIAN_POINT('Ctrl Pts',(180.292232490519,-2.33452396191265,339.328877560495));
#47542=CARTESIAN_POINT('Ctrl Pts',(180.284471239691,-2.21380770287781,339.393978731727));
#47543=CARTESIAN_POINT('Ctrl Pts',(180.276709988864,-2.09046203550478,339.453974961451));
#47544=CARTESIAN_POINT('Ctrl Pts',(180.268948738037,-1.96496339486667,339.508669639631));
#47545=CARTESIAN_POINT('Ctrl Pts',(180.26117507172,-1.8392639970223,339.563451811594));
#47546=CARTESIAN_POINT('Ctrl Pts',(180.253401405404,-1.71140510839831,339.612915343827));
#47547=CARTESIAN_POINT('Ctrl Pts',(180.245627739087,-1.58188067819185,339.656912773766));
#47548=CARTESIAN_POINT('Ctrl Pts',(180.238215891247,-1.45838484892414,339.698862381939));
#47549=CARTESIAN_POINT('Ctrl Pts',(180.230804043408,-1.33337530696609,339.735843184145));
#47550=CARTESIAN_POINT('Ctrl Pts',(180.223392195568,-1.20728826984767,339.767770767978));
#47551=CARTESIAN_POINT('Ctrl Pts',(180.215617114664,-1.07502207446831,339.801263029656));
#47552=CARTESIAN_POINT('Ctrl Pts',(180.207842033761,-0.941152118279231,
339.829300105866));
#47553=CARTESIAN_POINT('Ctrl Pts',(180.200066952857,-0.806168059987069,
339.851729188811));
#47554=CARTESIAN_POINT('Ctrl Pts',(180.19230143966,-0.671350107733285,339.874130671414));
#47555=CARTESIAN_POINT('Ctrl Pts',(180.184535926463,-0.535421163114858,
339.890937828256));
#47556=CARTESIAN_POINT('Ctrl Pts',(180.176770413267,-0.398884849820955,
339.902047933169));
#47557=CARTESIAN_POINT('Ctrl Pts',(180.169012599576,-0.262483912286073,
339.913147022412));
#47558=CARTESIAN_POINT('Ctrl Pts',(180.161254785886,-0.125477191576643,
339.918560269316));
#47559=CARTESIAN_POINT('Ctrl Pts',(180.153496972196,0.0116230674311581,
339.918236265858));
#47560=CARTESIAN_POINT('Ctrl Pts',(180.145744996487,0.148620154490342,339.917912506223));
#47561=CARTESIAN_POINT('Ctrl Pts',(180.137993020778,0.285710250440326,339.911860090816));
#47562=CARTESIAN_POINT('Ctrl Pts',(180.130241045069,0.422377935519294,339.900079585281));
#47563=CARTESIAN_POINT('Ctrl Pts',(180.122492352306,0.558987742110832,339.888304068766));
#47564=CARTESIAN_POINT('Ctrl Pts',(180.114743659543,0.695175105011753,339.870805320436));
#47565=CARTESIAN_POINT('Ctrl Pts',(180.10699496678,0.830426776348472,339.847635963191));
#47566=CARTESIAN_POINT('Ctrl Pts',(180.099247886186,0.96565030765392,339.824471426489));
#47567=CARTESIAN_POINT('Ctrl Pts',(180.091500805591,1.09993814960133,339.795638693551));
#47568=CARTESIAN_POINT('Ctrl Pts',(180.083753724997,1.23278472786932,339.761241946933));
#47569=CARTESIAN_POINT('Ctrl Pts',(180.076006579465,1.36563241968038,339.726844911995));
#47570=CARTESIAN_POINT('Ctrl Pts',(180.068259433933,1.49703844531977,339.686883868326));
#47571=CARTESIAN_POINT('Ctrl Pts',(180.060512288401,1.62651031850972,339.641513465054));
#47572=CARTESIAN_POINT('Ctrl Pts',(180.052763401139,1.75601129983935,339.596132861513));
#47573=CARTESIAN_POINT('Ctrl Pts',(180.045014513878,1.88357689462751,339.545340607619));
#47574=CARTESIAN_POINT('Ctrl Pts',(180.037265626616,2.0087329682738,339.48934014357));
#47575=CARTESIAN_POINT('Ctrl Pts',(180.029508514609,2.13402188381516,339.433280240075));
#47576=CARTESIAN_POINT('Ctrl Pts',(180.021751402602,2.25689581203898,339.372001243529));
#47577=CARTESIAN_POINT('Ctrl Pts',(180.013994290594,2.37690318911734,339.305753626494));
#47578=CARTESIAN_POINT('Ctrl Pts',(180.006233033433,2.49697469432843,339.239470608835));
#47579=CARTESIAN_POINT('Ctrl Pts',(179.998471776271,2.61417626233654,339.168213883172));
#47580=CARTESIAN_POINT('Ctrl Pts',(179.990710519109,2.72808473277588,339.09227769748));
#47581=CARTESIAN_POINT('Ctrl Pts',(179.982936846487,2.84217541933596,339.016220038845));
#47582=CARTESIAN_POINT('Ctrl Pts',(179.975163173864,2.95296216551882,338.935468192095));
#47583=CARTESIAN_POINT('Ctrl Pts',(179.967389501242,3.06005366223507,338.850357729711));
#47584=CARTESIAN_POINT('Ctrl Pts',(179.959977721259,3.16215966157294,338.769209467875));
#47585=CARTESIAN_POINT('Ctrl Pts',(179.952565941277,3.26090650290947,338.684099461569));
#47586=CARTESIAN_POINT('Ctrl Pts',(179.945154161294,3.35598714836865,338.595348845729));
#47587=CARTESIAN_POINT('Ctrl Pts',(179.937379082681,3.45572830296004,338.502247995899));
#47588=CARTESIAN_POINT('Ctrl Pts',(179.929604004068,3.55174996597638,338.404846397423));
#47589=CARTESIAN_POINT('Ctrl Pts',(179.921828925455,3.64365865570261,338.303473121311));
#47590=CARTESIAN_POINT('Ctrl Pts',(179.914063414568,3.73545424596446,338.202224591436));
#47591=CARTESIAN_POINT('Ctrl Pts',(179.906297903682,3.82314667338922,338.097014395261));
#47592=CARTESIAN_POINT('Ctrl Pts',(179.898532392796,3.90637701369591,337.98821044931));
#47593=CARTESIAN_POINT('Ctrl Pts',(179.890774581433,3.98952483090685,337.879514382751));
#47594=CARTESIAN_POINT('Ctrl Pts',(179.883016770071,4.06821912939376,337.767231965866));
#47595=CARTESIAN_POINT('Ctrl Pts',(179.875258958708,4.1421394739621,337.651766136134));
#47596=CARTESIAN_POINT('Ctrl Pts',(179.867506985342,4.21600419115477,337.536387198056));
#47597=CARTESIAN_POINT('Ctrl Pts',(179.859755011976,4.28510189532527,337.417829943359));
#47598=CARTESIAN_POINT('Ctrl Pts',(179.852003038609,4.34915413891717,337.296528105301));
#47599=CARTESIAN_POINT('Ctrl Pts',(179.844254348203,4.41317925638844,337.175277638563));
#47600=CARTESIAN_POINT('Ctrl Pts',(179.836505657797,4.47216298099564,337.051285245185));
#47601=CARTESIAN_POINT('Ctrl Pts',(179.828756967391,4.52587181656437,336.925011003223));
#47602=CARTESIAN_POINT('Ctrl Pts',(179.821009889162,4.57956947758329,336.798763033619));
#47603=CARTESIAN_POINT('Ctrl Pts',(179.813262810932,4.62799427964139,336.670234519221));
#47604=CARTESIAN_POINT('Ctrl Pts',(179.805515732702,4.67096023676915,336.539906987133));
#47605=CARTESIAN_POINT('Ctrl Pts',(179.797768589542,4.71392655401164,336.409578362718));
#47606=CARTESIAN_POINT('Ctrl Pts',(179.790021446381,4.75143381268354,336.277451061759));
#47607=CARTESIAN_POINT('Ctrl Pts',(179.78227430322,4.78334554792102,336.144022915716));
#47608=CARTESIAN_POINT('Ctrl Pts',(179.774525418333,4.81526445760872,336.010564772132));
#47609=CARTESIAN_POINT('Ctrl Pts',(179.766776533446,4.84158524968982,335.875805581584));
#47610=CARTESIAN_POINT('Ctrl Pts',(179.75902764856,4.86222241989627,335.74025414687));
#47611=CARTESIAN_POINT('Ctrl Pts',(179.75127053892,4.88288149462591,335.604558836348));
#47612=CARTESIAN_POINT('Ctrl Pts',(179.74351342928,4.89784483775294,335.468069988922));
#47613=CARTESIAN_POINT('Ctrl Pts',(179.735756319641,4.90707870986626,335.331302879066));
#47614=CARTESIAN_POINT('Ctrl Pts',(179.727995064846,4.91631751626959,335.19446268518));
#47615=CARTESIAN_POINT('Ctrl Pts',(179.720233810052,4.91982074107055,335.057344323124));
#47616=CARTESIAN_POINT('Ctrl Pts',(179.712472555257,4.91760682728085,334.920462871684));
#47617=CARTESIAN_POINT('Ctrl Pts',(179.704698884977,4.91538937194855,334.783362454404));
#47618=CARTESIAN_POINT('Ctrl Pts',(179.696925214697,4.90743652516739,334.646500095476));
#47619=CARTESIAN_POINT('Ctrl Pts',(179.689151544417,4.89381871716129,334.51038645233));
#47620=CARTESIAN_POINT('Ctrl Pts',(179.681739738618,4.88083481834485,334.380608901541));
#47621=CARTESIAN_POINT('Ctrl Pts',(179.67432793282,4.86270153481921,334.251512215092));
#47622=CARTESIAN_POINT('Ctrl Pts',(179.666916127021,4.83952276121924,334.123528376876));
#47623=CARTESIAN_POINT('Ctrl Pts',(179.659141048744,4.81520793376719,333.989271707539));
#47624=CARTESIAN_POINT('Ctrl Pts',(179.651365970466,4.78526368527593,333.85581545574));
#47625=CARTESIAN_POINT('Ctrl Pts',(179.643590892189,4.74975380296486,333.723668587819));
#47626=CARTESIAN_POINT('Ctrl Pts',(179.63582538165,4.71428761786355,333.591684335176));
#47627=CARTESIAN_POINT('Ctrl Pts',(179.62805987111,4.67326952670137,333.461006634296));
#47628=CARTESIAN_POINT('Ctrl Pts',(179.62029436057,4.62681468373114,333.332136412979));
#47629=CARTESIAN_POINT('Ctrl Pts',(179.612536549564,4.58040590091978,333.203393966992));
#47630=CARTESIAN_POINT('Ctrl Pts',(179.604778738559,4.52857122551935,333.076455799486));
#47631=CARTESIAN_POINT('Ctrl Pts',(179.597020927553,4.47147609030416,332.951809423823));
#47632=CARTESIAN_POINT('Ctrl Pts',(179.589268954553,4.41442392104135,332.827256848626));
#47633=CARTESIAN_POINT('Ctrl Pts',(179.581516981553,4.35211933362127,332.704992986379));
#47634=CARTESIAN_POINT('Ctrl Pts',(179.573765008554,4.28477637956999,332.585486707517));
#47635=CARTESIAN_POINT('Ctrl Pts',(179.566016318528,4.21746194537485,332.466031039767));
#47636=CARTESIAN_POINT('Ctrl Pts',(179.558267628502,4.14511357993295,332.349330972468));
#47637=CARTESIAN_POINT('Ctrl Pts',(179.550518938476,4.06799181444826,332.235831832163));
#47638=CARTESIAN_POINT('Ctrl Pts',(179.542771860635,3.99088609484248,332.122356306378));
#47639=CARTESIAN_POINT('Ctrl Pts',(179.535024782794,3.90900917017971,332.012080706));
#47640=CARTESIAN_POINT('Ctrl Pts',(179.527277704953,3.82266531912732,331.905422012545));
#47641=CARTESIAN_POINT('Ctrl Pts',(179.519530562188,3.73632074448113,331.79876242525));
#47642=CARTESIAN_POINT('Ctrl Pts',(179.511783419424,3.6455094147187,331.695720109138));
#47643=CARTESIAN_POINT('Ctrl Pts',(179.504036276659,3.5505761179036,331.596679225599));
#47644=CARTESIAN_POINT('Ctrl Pts',(179.496287392176,3.45562147811633,331.497616075616));
#47645=CARTESIAN_POINT('Ctrl Pts',(179.488538507694,3.35654329766334,331.402556430443));
#47646=CARTESIAN_POINT('Ctrl Pts',(179.480789623211,3.25372316834826,331.311847534842));
#47647=CARTESIAN_POINT('Ctrl Pts',(179.473032513985,3.15079390472287,331.221042359914));
#47648=CARTESIAN_POINT('Ctrl Pts',(179.465275404759,3.04411505188468,331.134597418299));
#47649=CARTESIAN_POINT('Ctrl Pts',(179.457518295533,2.93410165674349,331.052819926784));
#47650=CARTESIAN_POINT('Ctrl Pts',(179.449757041159,2.82402947399585,330.970998736017));
#47651=CARTESIAN_POINT('Ctrl Pts',(179.441995786784,2.71061952142621,330.893850184876));
#47652=CARTESIAN_POINT('Ctrl Pts',(179.434234532409,2.5943149202941,330.82163750294));
#47653=CARTESIAN_POINT('Ctrl Pts',(179.426460862555,2.47782426967704,330.74930930423));
#47654=CARTESIAN_POINT('Ctrl Pts',(179.418687192701,2.35843005798795,330.681932945038));
#47655=CARTESIAN_POINT('Ctrl Pts',(179.410913522847,2.23659982174236,330.619725545142));
#47656=CARTESIAN_POINT('Ctrl Pts',(179.403501712813,2.12044071229309,330.56041386361));
#47657=CARTESIAN_POINT('Ctrl Pts',(179.39608990278,2.00206752582918,330.505800869709));
#47658=CARTESIAN_POINT('Ctrl Pts',(179.388678092746,1.88189975092606,330.456032967773));
#47659=CARTESIAN_POINT('Ctrl Pts',(179.380903013634,1.75584228960839,330.403825831724));
#47660=CARTESIAN_POINT('Ctrl Pts',(179.373127934522,1.62741151364918,330.356785749238));
#47661=CARTESIAN_POINT('Ctrl Pts',(179.36535285541,1.49706994276828,330.315134511114));
#47662=CARTESIAN_POINT('Ctrl Pts',(179.357587344023,1.36688876541817,330.273534527467));
#47663=CARTESIAN_POINT('Ctrl Pts',(179.349821832637,1.23480184043307,330.23731031161));
#47664=CARTESIAN_POINT('Ctrl Pts',(179.34205632125,1.10129272539183,330.206636108587));
#47665=CARTESIAN_POINT('Ctrl Pts',(179.334298509387,0.967915984962775,330.175992319111));
#47666=CARTESIAN_POINT('Ctrl Pts',(179.326540697524,0.833120239161106,330.150887678444));
#47667=CARTESIAN_POINT('Ctrl Pts',(179.318782885661,0.697404973659279,330.131446892021));
#47668=CARTESIAN_POINT('Ctrl Pts',(179.311030911794,0.561791838141364,330.112020735398));
#47669=CARTESIAN_POINT('Ctrl Pts',(179.303278937927,0.425260945617152,330.098250004465));
#47670=CARTESIAN_POINT('Ctrl Pts',(179.29552696406,0.288322414907676,330.090208431353));
#47671=CARTESIAN_POINT('Ctrl Pts',(179.287778273155,0.151441877685195,330.082170263847));
#47672=CARTESIAN_POINT('Ctrl Pts',(179.280029582251,0.0141544350259075,
330.079856451289));
#47673=CARTESIAN_POINT('Ctrl Pts',(179.272280891346,-0.123024439995396,
330.083288899105));
#47674=CARTESIAN_POINT('Ctrl Pts',(179.264533812619,-0.260174773842745,
330.086720632772));
#47675=CARTESIAN_POINT('Ctrl Pts',(179.256786733891,-0.397216194475365,
330.095896238996));
#47676=CARTESIAN_POINT('Ctrl Pts',(179.249039655164,-0.533633390503498,
330.110785495906));
#47677=CARTESIAN_POINT('Ctrl Pts',(179.241292511508,-0.670051729868452,
330.125674877606));
#47678=CARTESIAN_POINT('Ctrl Pts',(179.233545367851,-0.805845445627147,
330.146277963096));
#47679=CARTESIAN_POINT('Ctrl Pts',(179.225798224194,-0.940504903583203,
330.172512704436));
#47680=CARTESIAN_POINT('Ctrl Pts',(179.218049338814,-1.07519463586621,330.198753343907));
#47681=CARTESIAN_POINT('Ctrl Pts',(179.210300453433,-1.20874921932831,330.230628083928));
#47682=CARTESIAN_POINT('Ctrl Pts',(179.202551568053,-1.34067014714226,330.268003949805));
#47683=CARTESIAN_POINT('Ctrl Pts',(179.194794457926,-1.47273109718822,330.305419486811));
#47684=CARTESIAN_POINT('Ctrl Pts',(179.187037347799,-1.60315455113459,330.34834770681));
#47685=CARTESIAN_POINT('Ctrl Pts',(179.179280237672,-1.73145755805979,330.396605840563));
#47686=CARTESIAN_POINT('Ctrl Pts',(179.171518982392,-1.85982912601693,330.444889761922));
#47687=CARTESIAN_POINT('Ctrl Pts',(179.163757727113,-1.98607762956232,330.49850911948));
#47688=CARTESIAN_POINT('Ctrl Pts',(179.155996471834,-2.10974191491704,330.557233731678));
#47689=CARTESIAN_POINT('Ctrl Pts',(179.148222801079,-2.23360402277776,330.616052284093));
#47690=CARTESIAN_POINT('Ctrl Pts',(179.140449130323,-2.35487330574006,330.679992228318));
#47691=CARTESIAN_POINT('Ctrl Pts',(179.132675459568,-2.47311417224835,330.748777898824));
#47692=CARTESIAN_POINT('Ctrl Pts',(179.125263659203,-2.58585083491068,330.814361543133));
#47693=CARTESIAN_POINT('Ctrl Pts',(179.117851858838,-2.69583444196028,330.884349769728));
#47694=CARTESIAN_POINT('Ctrl Pts',(179.110440058472,-2.80271487094277,330.958469050632));
#47695=CARTESIAN_POINT('Ctrl Pts',(179.102708382103,-2.91420800976325,331.035787146694));
#47696=CARTESIAN_POINT('Ctrl Pts',(179.094976705735,-3.02268519373827,331.117851338745));
#47697=CARTESIAN_POINT('Ctrl Pts',(179.087245029366,-3.12771237425401,331.204397496255));
#47698=CARTESIAN_POINT('Ctrl Pts',(179.079522891834,-3.23260997910968,331.29083687878));
#47699=CARTESIAN_POINT('Ctrl Pts',(179.071800754301,-3.33406574526876,331.381746977801));
#47700=CARTESIAN_POINT('Ctrl Pts',(179.064078616769,-3.43167398503973,331.47682008366));
#47701=CARTESIAN_POINT('Ctrl Pts',(179.056364106087,-3.5291858209934,331.571799289554));
#47702=CARTESIAN_POINT('Ctrl Pts',(179.048649595406,-3.62285740967042,331.670933047297));
#47703=CARTESIAN_POINT('Ctrl Pts',(179.040935084725,-3.712315934423,331.773873302933));
#47704=CARTESIAN_POINT('Ctrl Pts',(179.033226296048,-3.80170810603049,331.876737205759));
#47705=CARTESIAN_POINT('Ctrl Pts',(179.025517507371,-3.88689317395647,331.983401690286));
#47706=CARTESIAN_POINT('Ctrl Pts',(179.017808718694,-3.96753532506472,332.093482064933));
#47707=CARTESIAN_POINT('Ctrl Pts',(179.010103047342,-4.0481448656259,332.203517924632));
#47708=CARTESIAN_POINT('Ctrl Pts',(179.00239737599,-4.12421490884533,332.316966609159));
#47709=CARTESIAN_POINT('Ctrl Pts',(178.994691704638,-4.19545027138025,332.433410807536));
#47710=CARTESIAN_POINT('Ctrl Pts',(178.986987464531,-4.26667240272455,332.549833377674));
#47711=CARTESIAN_POINT('Ctrl Pts',(178.979283224423,-4.33306143284986,332.66925001773));
#47712=CARTESIAN_POINT('Ctrl Pts',(178.971578984316,-4.39436609070922,332.791215328891));
#47713=CARTESIAN_POINT('Ctrl Pts',(178.963874459602,-4.45567301325495,332.913185145635));
#47714=CARTESIAN_POINT('Ctrl Pts',(178.956169934889,-4.51189501222608,333.037703467143));
#47715=CARTESIAN_POINT('Ctrl Pts',(178.948465410175,-4.56282748927638,333.164301668137));
#47716=CARTESIAN_POINT('Ctrl Pts',(178.940758885133,-4.61377318993814,333.290932737853));
#47717=CARTESIAN_POINT('Ctrl Pts',(178.933052360092,-4.65942648923579,333.419644394199));
#47718=CARTESIAN_POINT('Ctrl Pts',(178.925345835051,-4.69963166973435,333.549949921096));
#47719=CARTESIAN_POINT('Ctrl Pts',(178.917631200045,-4.73987916017159,333.680392575069));
#47720=CARTESIAN_POINT('Ctrl Pts',(178.909916565038,-4.7746669667763,333.812432070305));
#47721=CARTESIAN_POINT('Ctrl Pts',(178.902201930032,-4.80388971657654,333.945568089695));
#47722=CARTESIAN_POINT('Ctrl Pts',(178.894482839354,-4.83312934429419,334.078781003242));
#47723=CARTESIAN_POINT('Ctrl Pts',(178.886763748677,-4.85679744504241,334.213091313241));
#47724=CARTESIAN_POINT('Ctrl Pts',(178.879044657999,-4.8748403203292,334.347991630581));
#47725=CARTESIAN_POINT('Ctrl Pts',(178.871314161668,-4.89290985559224,334.483091275311));
#47726=CARTESIAN_POINT('Ctrl Pts',(178.863583665338,-4.90533753073623,334.618782275072));
#47727=CARTESIAN_POINT('Ctrl Pts',(178.855853169007,-4.91212170826543,334.754554719566));
#47728=CARTESIAN_POINT('Ctrl Pts',(178.851174571521,-4.91622758123578,334.836725978729));
#47729=CARTESIAN_POINT('Ctrl Pts',(178.846495974035,-4.91826735198843,334.918927091343));
#47730=CARTESIAN_POINT('Ctrl Pts',(178.84181737655,-4.91824988879026,335.001045903734));
#47731=CARTESIAN_POINT('',(177.091817376539,-4.91824792695348,334.995484303182));
#47732=CARTESIAN_POINT('Ctrl Pts',(178.841817376508,-4.9182498887901,335.001045904463));
#47733=CARTESIAN_POINT('Ctrl Pts',(178.838612259072,-4.91823792545276,335.057302173198));
#47734=CARTESIAN_POINT('Ctrl Pts',(178.835407141635,-4.91726078409659,335.113547047247));
#47735=CARTESIAN_POINT('Ctrl Pts',(178.832202024199,-4.91531943401054,335.169758428769));
#47736=CARTESIAN_POINT('Ctrl Pts',(178.824426945485,-4.91061004347224,335.306117836682));
#47737=CARTESIAN_POINT('Ctrl Pts',(178.816651866771,-4.90021464528335,335.442496600396));
#47738=CARTESIAN_POINT('Ctrl Pts',(178.808876788057,-4.88412299907667,335.578381874189));
#47739=CARTESIAN_POINT('Ctrl Pts',(178.801111277073,-4.86805115466751,335.714099932481));
#47740=CARTESIAN_POINT('Ctrl Pts',(178.79334576609,-4.84629705485512,335.849325324696));
#47741=CARTESIAN_POINT('Ctrl Pts',(178.785580255107,-4.81890244856952,335.983545755759));
#47742=CARTESIAN_POINT('Ctrl Pts',(178.777822443651,-4.79153500411964,336.117633106854));
#47743=CARTESIAN_POINT('Ctrl Pts',(178.770064632195,-4.75853826040876,336.250717099221));
#47744=CARTESIAN_POINT('Ctrl Pts',(178.76230682074,-4.72000565339145,336.382291465087));
#47745=CARTESIAN_POINT('Ctrl Pts',(178.754554847284,-4.68150204338778,336.513766817054));
#47746=CARTESIAN_POINT('Ctrl Pts',(178.746802873829,-4.6374709715389,336.643734430148));
#47747=CARTESIAN_POINT('Ctrl Pts',(178.739050900373,-4.58805667201154,336.771699477031));
#47748=CARTESIAN_POINT('Ctrl Pts',(178.731302209885,-4.53866329947717,336.899610330619));
#47749=CARTESIAN_POINT('Ctrl Pts',(178.723553519396,-4.4838913741393,337.02551994091));
#47750=CARTESIAN_POINT('Ctrl Pts',(178.715804828907,-4.42393451805586,337.148950079098));
#47751=CARTESIAN_POINT('Ctrl Pts',(178.708057750598,-4.36399013650276,337.272354536603));
#47752=CARTESIAN_POINT('Ctrl Pts',(178.70031067229,-4.29886314063021,337.393280196748));
#47753=CARTESIAN_POINT('Ctrl Pts',(178.692563593982,-4.22879452873173,337.511270574086));
#47754=CARTESIAN_POINT('Ctrl Pts',(178.684816450746,-4.15872532959671,337.629261940286));
#47755=CARTESIAN_POINT('Ctrl Pts',(178.67706930751,-4.08371463141165,337.74431763853));
#47756=CARTESIAN_POINT('Ctrl Pts',(178.669322164275,-4.00404824948484,337.85600782182));
#47757=CARTESIAN_POINT('Ctrl Pts',(178.661573279317,-3.92436395686988,337.967723115426));
#47758=CARTESIAN_POINT('Ctrl Pts',(178.65382439436,-3.84002212463943,338.076071070295));
#47759=CARTESIAN_POINT('Ctrl Pts',(178.646075509403,-3.7513503086192,338.180653065728));
#47760=CARTESIAN_POINT('Ctrl Pts',(178.638318399699,-3.66258437542264,338.285346065565));
#47761=CARTESIAN_POINT('Ctrl Pts',(178.630561289996,-3.56947953089565,338.386264822521));
#47762=CARTESIAN_POINT('Ctrl Pts',(178.622804180292,-3.47240220618024,338.483045503724));
#47763=CARTESIAN_POINT('Ctrl Pts',(178.615042925438,-3.37527300645101,338.579877901425));
#47764=CARTESIAN_POINT('Ctrl Pts',(178.607281670583,-3.27416738470544,338.672567553242));
#47765=CARTESIAN_POINT('Ctrl Pts',(178.599520415729,-3.16948589351096,338.760790107588));
#47766=CARTESIAN_POINT('Ctrl Pts',(178.591746745396,-3.06463694604437,338.849153789272));
#47767=CARTESIAN_POINT('Ctrl Pts',(178.583973075063,-2.95620100775418,338.933035854573));
#47768=CARTESIAN_POINT('Ctrl Pts',(178.57619940473,-2.84460943769667,339.012154061033));
#47769=CARTESIAN_POINT('Ctrl Pts',(178.568787599795,-2.73821247020903,339.08758930436));
#47770=CARTESIAN_POINT('Ctrl Pts',(178.561375794859,-2.62894728930402,339.15869406513));
#47771=CARTESIAN_POINT('Ctrl Pts',(178.553963989924,-2.51720789974148,339.225263003883));
#47772=CARTESIAN_POINT('Ctrl Pts',(178.546188911095,-2.39999184105947,339.295094677939));
#47773=CARTESIAN_POINT('Ctrl Pts',(178.538413832265,-2.27968248062893,339.360155341192));
#47774=CARTESIAN_POINT('Ctrl Pts',(178.530638753435,-2.1567055397287,339.420158852055));
#47775=CARTESIAN_POINT('Ctrl Pts',(178.522873242334,-2.03387992977276,339.480088524784));
#47776=CARTESIAN_POINT('Ctrl Pts',(178.515107731234,-1.90839361876503,339.534973257639));
#47777=CARTESIAN_POINT('Ctrl Pts',(178.507342220133,-1.78069999932524,339.584570925932));
#47778=CARTESIAN_POINT('Ctrl Pts',(178.499584408558,-1.65313298847095,339.634119417997));
#47779=CARTESIAN_POINT('Ctrl Pts',(178.491826596984,-1.52336338653626,339.678391137045));
#47780=CARTESIAN_POINT('Ctrl Pts',(178.484068785409,-1.39186748846544,339.717190684831));
#47781=CARTESIAN_POINT('Ctrl Pts',(178.476316811833,-1.26047054521905,339.755961034729));
#47782=CARTESIAN_POINT('Ctrl Pts',(178.468564838257,-1.12735026500233,339.789267299835));
#47783=CARTESIAN_POINT('Ctrl Pts',(178.460812864682,-0.993000812081995,
339.816962990278));
#47784=CARTESIAN_POINT('Ctrl Pts',(178.453064174071,-0.858708256224505,
339.844646951581));
#47785=CARTESIAN_POINT('Ctrl Pts',(178.44531548346,-0.72318794503902,339.866724985326));
#47786=CARTESIAN_POINT('Ctrl Pts',(178.437566792849,-0.586946811351083,
339.883101115392));
#47787=CARTESIAN_POINT('Ctrl Pts',(178.429819714417,-0.450734023762842,
339.899473838269));
#47788=CARTESIAN_POINT('Ctrl Pts',(178.422072635985,-0.313801099816476,
339.91014697054));
#47789=CARTESIAN_POINT('Ctrl Pts',(178.414325557554,-0.176662325884397,
339.915076142351));
#47790=CARTESIAN_POINT('Ctrl Pts',(178.406578414194,-0.0395224025923842,
339.920005355474));
#47791=CARTESIAN_POINT('Ctrl Pts',(178.398831270834,0.0978229835043959,
339.919190498078));
#47792=CARTESIAN_POINT('Ctrl Pts',(178.391084127474,0.234857693818518,339.912639303486));
#47793=CARTESIAN_POINT('Ctrl Pts',(178.383335242392,0.371923212448787,339.906086636046));
#47794=CARTESIAN_POINT('Ctrl Pts',(178.37558635731,0.508677525957545,339.893795083812));
#47795=CARTESIAN_POINT('Ctrl Pts',(178.367837472227,0.644608166431105,339.87582437894));
#47796=CARTESIAN_POINT('Ctrl Pts',(178.360080362398,0.780683085091036,339.857834599778));
#47797=CARTESIAN_POINT('Ctrl Pts',(178.352323252569,0.915932196194659,339.83415367797));
#47798=CARTESIAN_POINT('Ctrl Pts',(178.34456614274,1.0498512479887,339.804892862447));
#47799=CARTESIAN_POINT('Ctrl Pts',(178.336804887759,1.18384186184367,339.77561641088));
#47800=CARTESIAN_POINT('Ctrl Pts',(178.329043632779,1.31650062232678,339.740754223554));
#47801=CARTESIAN_POINT('Ctrl Pts',(178.321282377798,1.44733801327893,339.700467608421));
#47802=CARTESIAN_POINT('Ctrl Pts',(178.313508707339,1.5783847014096,339.660116547836));
#47803=CARTESIAN_POINT('Ctrl Pts',(178.305735036881,1.70760382916077,339.614323850227));
#47804=CARTESIAN_POINT('Ctrl Pts',(178.297961366422,1.834524619681,339.563299517047));
#47805=CARTESIAN_POINT('Ctrl Pts',(178.290549562831,1.95553720644523,339.514650383042));
#47806=CARTESIAN_POINT('Ctrl Pts',(178.283137759241,2.07446035361744,339.461245836355));
#47807=CARTESIAN_POINT('Ctrl Pts',(178.275725955651,2.19090816849813,339.4033060829));
#47808=CARTESIAN_POINT('Ctrl Pts',(178.267950876883,2.31306344715932,339.342526524813));
#47809=CARTESIAN_POINT('Ctrl Pts',(178.260175798116,2.43288064419288,339.276563875661));
#47810=CARTESIAN_POINT('Ctrl Pts',(178.252400719349,2.54988875482794,339.20562128591));
#47811=CARTESIAN_POINT('Ctrl Pts',(178.244635208311,2.66675287953293,339.134765995533));
#47812=CARTESIAN_POINT('Ctrl Pts',(178.236869697274,2.78081446475652,339.058943158501));
#47813=CARTESIAN_POINT('Ctrl Pts',(178.229104186236,2.89162454592362,338.978403014768));
#47814=CARTESIAN_POINT('Ctrl Pts',(178.221346374725,3.002324758572,338.897942726822));
#47815=CARTESIAN_POINT('Ctrl Pts',(178.213588563214,3.10977956871502,338.812774668443));
#47816=CARTESIAN_POINT('Ctrl Pts',(178.205830751703,3.21356691127736,338.723193625));
#47817=CARTESIAN_POINT('Ctrl Pts',(178.198078778192,3.3172761505726,338.633679994134));
#47818=CARTESIAN_POINT('Ctrl Pts',(178.19032680468,3.41732312099803,338.539760242682));
#47819=CARTESIAN_POINT('Ctrl Pts',(178.182574831168,3.5133172154582,338.441770649835));
#47820=CARTESIAN_POINT('Ctrl Pts',(178.174826140622,3.60927065636261,338.343822555639));
#47821=CARTESIAN_POINT('Ctrl Pts',(178.167077450076,3.7011743621283,338.241808326765));
#47822=CARTESIAN_POINT('Ctrl Pts',(178.159328759529,3.7886732939505,338.136102315647));
#47823=CARTESIAN_POINT('Ctrl Pts',(178.151581681163,3.87615402088921,338.030418297548));
#47824=CARTESIAN_POINT('Ctrl Pts',(178.143834602796,3.95923154768538,337.921044325935));
#47825=CARTESIAN_POINT('Ctrl Pts',(178.13608752443,4.03759025291669,337.808388864109));
#47826=CARTESIAN_POINT('Ctrl Pts',(178.128340381135,4.11594961486958,337.695732458122));
#47827=CARTESIAN_POINT('Ctrl Pts',(178.120593237841,4.18958985318097,337.57979482795));
#47828=CARTESIAN_POINT('Ctrl Pts',(178.112846094546,4.25823815876292,337.461014190482));
#47829=CARTESIAN_POINT('Ctrl Pts',(178.105097209529,4.3269018979417,337.342206848605));
#47830=CARTESIAN_POINT('Ctrl Pts',(178.097348324513,4.39057127560532,337.220555565911));
#47831=CARTESIAN_POINT('Ctrl Pts',(178.089599439496,4.44901919600697,337.096523612093));
#47832=CARTESIAN_POINT('Ctrl Pts',(178.081842329732,4.5075291536362,336.972360009475));
#47833=CARTESIAN_POINT('Ctrl Pts',(178.074085219969,4.56080641623842,336.845811042217));
#47834=CARTESIAN_POINT('Ctrl Pts',(178.066328110205,4.60867165585424,336.717360949546));
#47835=CARTESIAN_POINT('Ctrl Pts',(178.05856685529,4.65656247312396,336.588842217252));
#47836=CARTESIAN_POINT('Ctrl Pts',(178.050805600375,4.69903538383889,336.458420706747));
#47837=CARTESIAN_POINT('Ctrl Pts',(178.04304434546,4.73596113001569,336.326595355593));
#47838=CARTESIAN_POINT('Ctrl Pts',(178.035270675066,4.77294594535329,336.194559126835));
#47839=CARTESIAN_POINT('Ctrl Pts',(178.027497004672,4.80436577433105,336.061114950551));
#47840=CARTESIAN_POINT('Ctrl Pts',(178.019723334279,4.83014244728336,335.926772356866));
#47841=CARTESIAN_POINT('Ctrl Pts',(178.012311529978,4.85471921035278,335.798683440922));
#47842=CARTESIAN_POINT('Ctrl Pts',(178.004899725677,4.8741663288044,335.669778152457));
#47843=CARTESIAN_POINT('Ctrl Pts',(177.997487921376,4.88846014980437,335.540500163066));
#47844=CARTESIAN_POINT('Ctrl Pts',(177.989712842606,4.90345455328522,335.404885876716));
#47845=CARTESIAN_POINT('Ctrl Pts',(177.981937763835,4.91282511478255,335.268432865106));
#47846=CARTESIAN_POINT('Ctrl Pts',(177.974162685065,4.91648778014887,335.13164714257));
#47847=CARTESIAN_POINT('Ctrl Pts',(177.966397174024,4.9201459383722,334.995029743576));
#47848=CARTESIAN_POINT('Ctrl Pts',(177.958631662983,4.91811016570806,334.858080835288));
#47849=CARTESIAN_POINT('Ctrl Pts',(177.950866151942,4.91034793377973,334.721313380793));
#47850=CARTESIAN_POINT('Ctrl Pts',(177.943108340428,4.9025933981271,334.58468153163));
#47851=CARTESIAN_POINT('Ctrl Pts',(177.935350528914,4.88912372436133,334.448231165957));
#47852=CARTESIAN_POINT('Ctrl Pts',(177.9275927174,4.86995840015661,334.31247673258));
#47853=CARTESIAN_POINT('Ctrl Pts',(177.919840743885,4.85080749846647,334.176824458721));
#47854=CARTESIAN_POINT('Ctrl Pts',(177.912088770371,4.82596953214509,334.041867460213));
#47855=CARTESIAN_POINT('Ctrl Pts',(177.904336796856,4.79551590562572,333.908116186863));
#47856=CARTESIAN_POINT('Ctrl Pts',(177.896588106307,4.76507517623592,333.774421557259));
#47857=CARTESIAN_POINT('Ctrl Pts',(177.888839415758,4.72902360338711,333.641932017542));
#47858=CARTESIAN_POINT('Ctrl Pts',(177.881090725209,4.68748385615793,333.511148710999));
#47859=CARTESIAN_POINT('Ctrl Pts',(177.873343646839,4.64595275162066,333.380392615018));
#47860=CARTESIAN_POINT('Ctrl Pts',(177.86559656847,4.59893586219554,333.251342418399));
#47861=CARTESIAN_POINT('Ctrl Pts',(177.857849490101,4.54660587252341,333.12448457686));
#47862=CARTESIAN_POINT('Ctrl Pts',(177.850102346804,4.4942754442762,332.997625672132));
#47863=CARTESIAN_POINT('Ctrl Pts',(177.842355203507,4.43663197602107,332.87295952047));
#47864=CARTESIAN_POINT('Ctrl Pts',(177.83460806021,4.37389634103569,332.75095267716));
#47865=CARTESIAN_POINT('Ctrl Pts',(177.82685917519,4.31114660174834,332.628918404122));
#47866=CARTESIAN_POINT('Ctrl Pts',(177.819110290171,4.24330259635909,332.509544976673));
#47867=CARTESIAN_POINT('Ctrl Pts',(177.811361405152,4.170631003696,332.393274066284));
#47868=CARTESIAN_POINT('Ctrl Pts',(177.803604295386,4.09788227665428,332.27687974475));
#47869=CARTESIAN_POINT('Ctrl Pts',(177.79584718562,4.02029593406106,332.163594850421));
#47870=CARTESIAN_POINT('Ctrl Pts',(177.788090075854,3.93818213836565,332.053832233637));
#47871=CARTESIAN_POINT('Ctrl Pts',(177.780328820937,3.8560244636839,331.944010963221));
#47872=CARTESIAN_POINT('Ctrl Pts',(177.77256756602,3.76933476208939,331.837716023543));
#47873=CARTESIAN_POINT('Ctrl Pts',(177.764806311102,3.67846265191155,331.735326114144));
#47874=CARTESIAN_POINT('Ctrl Pts',(177.757032640707,3.58744517597258,331.632772414259));
#47875=CARTESIAN_POINT('Ctrl Pts',(177.749258970311,3.49223219347847,331.534136508935));
#47876=CARTESIAN_POINT('Ctrl Pts',(177.741485299915,3.39320987709146,331.439759868701));
#47877=CARTESIAN_POINT('Ctrl Pts',(177.734073495644,3.29879707205368,331.349776482535));
#47878=CARTESIAN_POINT('Ctrl Pts',(177.726661691373,3.20092181693157,331.263664937921));
#47879=CARTESIAN_POINT('Ctrl Pts',(177.719249887103,3.09994440472266,331.181685221183));
#47880=CARTESIAN_POINT('Ctrl Pts',(177.711474808317,2.99401778997952,331.095687435326));
#47881=CARTESIAN_POINT('Ctrl Pts',(177.70369972953,2.88434248966918,331.013964975834));
#47882=CARTESIAN_POINT('Ctrl Pts',(177.695924650744,2.77129853552137,330.936862359024));
#47883=CARTESIAN_POINT('Ctrl Pts',(177.688159139687,2.65839368915438,330.859854621891));
#47884=CARTESIAN_POINT('Ctrl Pts',(177.680393628631,2.54212875682175,330.787455634041));
#47885=CARTESIAN_POINT('Ctrl Pts',(177.672628117574,2.42291749715954,330.71997034304));
#47886=CARTESIAN_POINT('Ctrl Pts',(177.664870306044,2.3038244358069,330.6525519639));
#47887=CARTESIAN_POINT('Ctrl Pts',(177.657112494514,2.18179119862214,330.590037777483));
#47888=CARTESIAN_POINT('Ctrl Pts',(177.649354682984,2.05726094248102,330.532689793954));
#47889=CARTESIAN_POINT('Ctrl Pts',(177.641602709453,1.93282439930542,330.4753849666));
#47890=CARTESIAN_POINT('Ctrl Pts',(177.633850735922,1.80589493100876,330.423238766636));
#47891=CARTESIAN_POINT('Ctrl Pts',(177.626098762391,1.67694042676136,330.376467382229));
#47892=CARTESIAN_POINT('Ctrl Pts',(177.618350071825,1.54804053482146,330.32971580553));
#47893=CARTESIAN_POINT('Ctrl Pts',(177.610601381259,1.41711767933166,330.288334650108));
#47894=CARTESIAN_POINT('Ctrl Pts',(177.602852690694,1.28465966565384,330.252491958307));
#47895=CARTESIAN_POINT('Ctrl Pts',(177.595105612308,1.15222921097109,330.216656723876));
#47896=CARTESIAN_POINT('Ctrl Pts',(177.587358533922,1.01826461048224,330.186357763046));
#47897=CARTESIAN_POINT('Ctrl Pts',(177.579611455536,0.883268384747759,330.161713110717));
#47898=CARTESIAN_POINT('Ctrl Pts',(177.571864312222,0.748271027614099,330.137068251843));
#47899=CARTESIAN_POINT('Ctrl Pts',(177.564117168908,0.612242412508957,330.118077866188));
#47900=CARTESIAN_POINT('Ctrl Pts',(177.556370025594,0.475694402931241,330.104808696535));
#47901=CARTESIAN_POINT('Ctrl Pts',(177.548621140558,0.339115694461391,330.091536543691));
#47902=CARTESIAN_POINT('Ctrl Pts',(177.540872255521,0.202017748123602,330.083988204144));
#47903=CARTESIAN_POINT('Ctrl Pts',(177.533123370485,0.0649162900988813,
330.082178435752));
#47904=CARTESIAN_POINT('Ctrl Pts',(177.525366260702,-0.0723306888300711,
330.080366746454));
#47905=CARTESIAN_POINT('Ctrl Pts',(177.517609150919,-0.209580795434104,
330.08430580078));
#47906=CARTESIAN_POINT('Ctrl Pts',(177.509852041136,-0.34631900835463,330.093958193518));
#47907=CARTESIAN_POINT('Ctrl Pts',(177.502090786202,-0.483130289804384,
330.103615744185));
#47908=CARTESIAN_POINT('Ctrl Pts',(177.494329531267,-0.619428744305054,
330.118992672895));
#47909=CARTESIAN_POINT('Ctrl Pts',(177.486568276333,-0.75470671679276,330.139999914184));
#47910=CARTESIAN_POINT('Ctrl Pts',(177.47879460592,-0.890201089948413,330.161040760214));
#47911=CARTESIAN_POINT('Ctrl Pts',(177.471020935507,-1.02467133539786,330.187729840673));
#47912=CARTESIAN_POINT('Ctrl Pts',(177.463247265095,-1.15762132310105,330.219927204027));
#47913=CARTESIAN_POINT('Ctrl Pts',(177.455835461006,-1.28438245524558,330.250625771972));
#47914=CARTESIAN_POINT('Ctrl Pts',(177.448423656917,-1.4097614037054,330.28633126344));
#47915=CARTESIAN_POINT('Ctrl Pts',(177.441011852828,-1.53334456524882,330.326881393895));
#47916=CARTESIAN_POINT('Ctrl Pts',(177.433236774052,-1.66298490718434,330.369419007532));
#47917=CARTESIAN_POINT('Ctrl Pts',(177.425461695276,-1.79105866483917,330.417422595237));
#47918=CARTESIAN_POINT('Ctrl Pts',(177.4176866165,-1.9170704701182,330.470759017771));
#47919=CARTESIAN_POINT('Ctrl Pts',(177.409921105453,-2.04292720984825,330.524029806442));
#47920=CARTESIAN_POINT('Ctrl Pts',(177.402155594406,-2.16672668931163,330.582620221759));
#47921=CARTESIAN_POINT('Ctrl Pts',(177.394390083359,-2.28798856305544,330.646347349888));
#47922=CARTESIAN_POINT('Ctrl Pts',(177.386632271839,-2.40913020529838,330.710011292383));
#47923=CARTESIAN_POINT('Ctrl Pts',(177.378874460319,-2.52773890511602,330.778801631536));
#47924=CARTESIAN_POINT('Ctrl Pts',(177.371116648799,-2.64335451495748,330.85248749601));
#47925=CARTESIAN_POINT('Ctrl Pts',(177.363364675279,-2.7588831203857,330.926117909534));
#47926=CARTESIAN_POINT('Ctrl Pts',(177.355612701758,-2.87142279082685,331.00463630625));
#47927=CARTESIAN_POINT('Ctrl Pts',(177.347860728237,-2.98053852736156,331.087766219995));
#47928=CARTESIAN_POINT('Ctrl Pts',(177.340112037682,-3.08960805331701,331.170860928172));
#47929=CARTESIAN_POINT('Ctrl Pts',(177.332363347126,-3.1952562191147,331.258563032656));
#47930=CARTESIAN_POINT('Ctrl Pts',(177.324614656571,-3.29707773489245,331.350553264867));
#47931=CARTESIAN_POINT('Ctrl Pts',(177.316867578195,-3.3988780658534,331.442524357741));
#47932=CARTESIAN_POINT('Ctrl Pts',(177.30912049982,-3.49685304057089,331.538781541862));
#47933=CARTESIAN_POINT('Ctrl Pts',(177.301373421444,-3.59063145826818,331.63896611243));
#47934=CARTESIAN_POINT('Ctrl Pts',(177.293626278141,-3.68441066191886,331.739151522641));
#47935=CARTESIAN_POINT('Ctrl Pts',(177.285879134837,-3.77399297128208,331.843264099588));
#47936=CARTESIAN_POINT('Ctrl Pts',(177.278131991534,-3.85904526221765,331.950909524685));
#47937=CARTESIAN_POINT('Ctrl Pts',(177.270383106508,-3.94411667471395,332.05857915076));
#47938=CARTESIAN_POINT('Ctrl Pts',(177.262634221482,-4.02465579991533,332.169782898837));
#47939=CARTESIAN_POINT('Ctrl Pts',(177.254885336456,-4.10037113859408,332.284095070095));
#47940=CARTESIAN_POINT('Ctrl Pts',(177.247128226684,-4.17616684231572,332.398528573472));
#47941=CARTESIAN_POINT('Ctrl Pts',(177.239371116911,-4.24712831561527,332.516076764328));
#47942=CARTESIAN_POINT('Ctrl Pts',(177.231614007139,-4.31300830572589,332.636286308108));
#47943=CARTESIAN_POINT('Ctrl Pts',(177.223852752215,-4.37892349999687,332.756560088024));
#47944=CARTESIAN_POINT('Ctrl Pts',(177.216091497291,-4.43975162718117,332.879497704452));
#47945=CARTESIAN_POINT('Ctrl Pts',(177.208330242367,-4.4952928630415,333.004624060988));
#47946=CARTESIAN_POINT('Ctrl Pts',(177.200556571964,-4.55092294677859,333.129950578916));
#47947=CARTESIAN_POINT('Ctrl Pts',(177.192782901562,-4.60124909543224,333.257472469751));
#47948=CARTESIAN_POINT('Ctrl Pts',(177.185009231159,-4.64612051280132,333.386696791354));
#47949=CARTESIAN_POINT('Ctrl Pts',(177.177597426958,-4.68890315504944,333.509905690138));
#47950=CARTESIAN_POINT('Ctrl Pts',(177.170185622756,-4.72672738943699,333.634661814839));
#47951=CARTESIAN_POINT('Ctrl Pts',(177.162773818555,-4.75950586004737,333.760529536183));
#47952=CARTESIAN_POINT('Ctrl Pts',(177.152670117745,-4.80418915861181,333.932111213659));
#47953=CARTESIAN_POINT('Ctrl Pts',(177.142566416936,-4.8396124932973,334.106196656317));
#47954=CARTESIAN_POINT('Ctrl Pts',(177.132462716126,-4.86554630448217,334.281917677811));
#47955=CARTESIAN_POINT('Ctrl Pts',(177.122563772259,-4.89095455300756,334.454077618108));
#47956=CARTESIAN_POINT('Ctrl Pts',(177.112664828391,-4.90725404236607,334.627807747289));
#47957=CARTESIAN_POINT('Ctrl Pts',(177.102765884524,-4.91427367871666,334.802269695867));
#47958=CARTESIAN_POINT('Ctrl Pts',(177.099116381862,-4.91686164990708,334.866589622739));
#47959=CARTESIAN_POINT('Ctrl Pts',(177.0954668792,-4.91818872865841,334.931008785057));
#47960=CARTESIAN_POINT('Ctrl Pts',(177.091817376539,-4.91824792695348,334.995484303182));
#47961=CARTESIAN_POINT('',(175.341817376454,-4.91824985388346,335.001198864178));
#47962=CARTESIAN_POINT('Ctrl Pts',(177.091817376508,-4.91824792695398,334.995484303725));
#47963=CARTESIAN_POINT('Ctrl Pts',(177.084148538999,-4.91837232254791,335.13096914033));
#47964=CARTESIAN_POINT('Ctrl Pts',(177.076479701491,-4.91289412939069,335.266594157412));
#47965=CARTESIAN_POINT('Ctrl Pts',(177.068810863982,-4.90180544779519,335.401853722722));
#47966=CARTESIAN_POINT('Ctrl Pts',(177.061132735662,-4.89070333223931,335.537277155271));
#47967=CARTESIAN_POINT('Ctrl Pts',(177.053454607341,-4.87397710942963,335.672333847374));
#47968=CARTESIAN_POINT('Ctrl Pts',(177.04577647902,-4.85167123739451,335.806516749199));
#47969=CARTESIAN_POINT('Ctrl Pts',(177.038114233037,-4.82941150543142,335.940422091431));
#47970=CARTESIAN_POINT('Ctrl Pts',(177.030451987054,-4.80159524579017,336.073456857911));
#47971=CARTESIAN_POINT('Ctrl Pts',(177.022789741071,-4.76831839161924,336.20512355327));
#47972=CARTESIAN_POINT('Ctrl Pts',(177.015127988233,-4.73504367916306,336.336781774496));
#47973=CARTESIAN_POINT('Ctrl Pts',(177.007466235396,-4.6963091691295,336.467071711546));
#47974=CARTESIAN_POINT('Ctrl Pts',(176.999804482559,-4.65226142676251,336.59550828251));
#47975=CARTESIAN_POINT('Ctrl Pts',(176.992141475785,-4.60820647545964,336.723965873643));
#47976=CARTESIAN_POINT('Ctrl Pts',(176.984478469011,-4.55883669257436,336.850569116841));
#47977=CARTESIAN_POINT('Ctrl Pts',(176.976815462237,-4.50434762908291,336.97485075357));
#47978=CARTESIAN_POINT('Ctrl Pts',(176.969125489074,-4.44966681667031,337.099569741727));
#47979=CARTESIAN_POINT('Ctrl Pts',(176.961435515911,-4.38983079202168,337.221950383105));
#47980=CARTESIAN_POINT('Ctrl Pts',(176.953745542748,-4.32508420336451,337.341544297319));
#47981=CARTESIAN_POINT('Ctrl Pts',(176.946070909403,-4.26046677002372,337.46089964777));
#47982=CARTESIAN_POINT('Ctrl Pts',(176.938396276059,-4.19095858995303,337.577479057295));
#47983=CARTESIAN_POINT('Ctrl Pts',(176.930721642714,-4.11684648137234,337.690865680652));
#47984=CARTESIAN_POINT('Ctrl Pts',(176.923023999642,-4.04251217332467,337.804592254495));
#47985=CARTESIAN_POINT('Ctrl Pts',(176.91532635657,-3.9635465404106,337.915106551997));
#47986=CARTESIAN_POINT('Ctrl Pts',(176.907628713498,-3.88027923995974,338.022021853402));
#47987=CARTESIAN_POINT('Ctrl Pts',(176.899931070425,-3.79701193950888,338.128937154806));
#47988=CARTESIAN_POINT('Ctrl Pts',(176.892233427353,-3.70944327822093,338.232253196925));
#47989=CARTESIAN_POINT('Ctrl Pts',(176.884535784281,-3.61793887719243,338.331621428584));
#47990=CARTESIAN_POINT('Ctrl Pts',(176.876760705501,-3.52551397258233,338.431989271323));
#47991=CARTESIAN_POINT('Ctrl Pts',(176.868985626722,-3.42876328950201,338.528666761841));
#47992=CARTESIAN_POINT('Ctrl Pts',(176.861210547942,-3.32801323321346,338.621258204279));
#47993=CARTESIAN_POINT('Ctrl Pts',(176.853445036892,-3.22738715628303,338.713735707053));
#47994=CARTESIAN_POINT('Ctrl Pts',(176.845679525842,-3.12277178353067,338.802136904345));
#47995=CARTESIAN_POINT('Ctrl Pts',(176.837914014792,-3.01453259830653,338.886100394515));
#47996=CARTESIAN_POINT('Ctrl Pts',(176.830156203268,-2.90640073254962,338.969980634639));
#47997=CARTESIAN_POINT('Ctrl Pts',(176.822398391745,-2.79465251149058,339.049431685854));
#47998=CARTESIAN_POINT('Ctrl Pts',(176.814640580222,-2.67968869865466,339.124130398133));
#47999=CARTESIAN_POINT('Ctrl Pts',(176.806888606698,-2.56481139973323,339.198772897262));
#48000=CARTESIAN_POINT('Ctrl Pts',(176.799136633173,-2.44672365204024,339.268669963769));
#48001=CARTESIAN_POINT('Ctrl Pts',(176.791384659649,-2.32585729783566,339.333540226259));
#48002=CARTESIAN_POINT('Ctrl Pts',(176.78363596909,-2.20504213060369,339.398383016155));
#48003=CARTESIAN_POINT('Ctrl Pts',(176.775887278532,-2.08145104100421,339.458203051714));
#48004=CARTESIAN_POINT('Ctrl Pts',(176.768138587973,-1.95554251917341,339.512763733922));
#48005=CARTESIAN_POINT('Ctrl Pts',(176.760391509594,-1.82966019366203,339.567313064325));
#48006=CARTESIAN_POINT('Ctrl Pts',(176.752644431215,-1.70146175339532,339.616605062603));
#48007=CARTESIAN_POINT('Ctrl Pts',(176.744897352836,-1.57142745803403,339.660450493958));
#48008=CARTESIAN_POINT('Ctrl Pts',(176.737150209529,-1.44139207285996,339.70429629278));
#48009=CARTESIAN_POINT('Ctrl Pts',(176.729403066222,-1.30952117228818,339.742695308744));
#48010=CARTESIAN_POINT('Ctrl Pts',(176.721655922915,-1.1763116545147,339.775507716877));
#48011=CARTESIAN_POINT('Ctrl Pts',(176.713907037885,-1.04307218841358,339.808327501936));
#48012=CARTESIAN_POINT('Ctrl Pts',(176.706158152856,-0.908493885710526,
339.835558086421));
#48013=CARTESIAN_POINT('Ctrl Pts',(176.698409267827,-0.773084959967538,
339.857110530673));
#48014=CARTESIAN_POINT('Ctrl Pts',(176.690652158051,-0.637532309791568,
339.878685850912));
#48015=CARTESIAN_POINT('Ctrl Pts',(176.682895048275,-0.501147662058251,
339.894570930208));
#48016=CARTESIAN_POINT('Ctrl Pts',(176.675137938499,-0.364446051565146,
339.90472854886));
#48017=CARTESIAN_POINT('Ctrl Pts',(176.667376683572,-0.227671392102332,
339.914891595417));
#48018=CARTESIAN_POINT('Ctrl Pts',(176.659615428644,-0.0905798228575022,
339.919321070248));
#48019=CARTESIAN_POINT('Ctrl Pts',(176.651854173717,0.0463134645227931,
339.918031936202));
#48020=CARTESIAN_POINT('Ctrl Pts',(176.644080503311,0.183425736549433,339.916740739962));
#48021=CARTESIAN_POINT('Ctrl Pts',(176.636306832905,0.320338702313612,339.909712674659));
#48022=CARTESIAN_POINT('Ctrl Pts',(176.628533162499,0.456541240209833,339.897014719039));
#48023=CARTESIAN_POINT('Ctrl Pts',(176.621121358335,0.586403516950871,339.884907856332));
#48024=CARTESIAN_POINT('Ctrl Pts',(176.613709554171,0.715619732940218,339.867647128908));
#48025=CARTESIAN_POINT('Ctrl Pts',(176.606297750007,0.843757212542922,339.845333510583));
#48026=CARTESIAN_POINT('Ctrl Pts',(176.598522671229,0.978175091951562,339.821926235316));
#48027=CARTESIAN_POINT('Ctrl Pts',(176.590747592451,1.11183060239176,339.792884259309));
#48028=CARTESIAN_POINT('Ctrl Pts',(176.582972513673,1.2442143581582,339.758267929978));
#48029=CARTESIAN_POINT('Ctrl Pts',(176.575207002624,1.37643520728524,339.723694198243));
#48030=CARTESIAN_POINT('Ctrl Pts',(176.567441491576,1.50738704104545,339.683559859752));
#48031=CARTESIAN_POINT('Ctrl Pts',(176.559675980527,1.63656816507568,339.637976682085));
#48032=CARTESIAN_POINT('Ctrl Pts',(176.551918169005,1.76562120564498,339.592438700271));
#48033=CARTESIAN_POINT('Ctrl Pts',(176.544160357483,1.89290666412929,339.541462759868));
#48034=CARTESIAN_POINT('Ctrl Pts',(176.536402545962,2.01793592063853,339.485210996452));
#48035=CARTESIAN_POINT('Ctrl Pts',(176.528650572439,2.14287108866756,339.429001564273));
#48036=CARTESIAN_POINT('Ctrl Pts',(176.520898598916,2.26555307921234,339.367524371346));
#48037=CARTESIAN_POINT('Ctrl Pts',(176.513146625394,2.38551158643912,339.300990296835));
#48038=CARTESIAN_POINT('Ctrl Pts',(176.505397934837,2.50541929116682,339.234484399543));
#48039=CARTESIAN_POINT('Ctrl Pts',(176.497649244279,2.62260546549487,339.162926069337));
#48040=CARTESIAN_POINT('Ctrl Pts',(176.489900553722,2.73662303294255,339.086572823047));
#48041=CARTESIAN_POINT('Ctrl Pts',(176.482153475345,2.85061687808291,339.010235462689));
#48042=CARTESIAN_POINT('Ctrl Pts',(176.474406396967,2.96144310307452,338.929105387943));
#48043=CARTESIAN_POINT('Ctrl Pts',(176.46665931859,3.0686826802779,338.843484053598));
#48044=CARTESIAN_POINT('Ctrl Pts',(176.458912175284,3.17592315625227,338.757862001663));
#48045=CARTESIAN_POINT('Ctrl Pts',(176.451165031979,3.27957661902429,338.667748858932));
#48046=CARTESIAN_POINT('Ctrl Pts',(176.443417888674,3.37925658666645,338.573486810382));
#48047=CARTESIAN_POINT('Ctrl Pts',(176.435669003646,3.47895896448144,338.479203569722));
#48048=CARTESIAN_POINT('Ctrl Pts',(176.427920118618,3.57468578560278,338.380769835663));
#48049=CARTESIAN_POINT('Ctrl Pts',(176.420171233591,3.66608723525464,338.278564845478));
#48050=CARTESIAN_POINT('Ctrl Pts',(176.412414123816,3.75758569934959,338.17625137386));
#48051=CARTESIAN_POINT('Ctrl Pts',(176.404657014042,3.84474936006083,338.070158941868));
#48052=CARTESIAN_POINT('Ctrl Pts',(176.396899904268,3.92726820366388,337.960700511533));
#48053=CARTESIAN_POINT('Ctrl Pts',(176.389138649342,4.00983114269864,337.851183590112));
#48054=CARTESIAN_POINT('Ctrl Pts',(176.381377394416,4.0877440970172,337.738297407841));
#48055=CARTESIAN_POINT('Ctrl Pts',(176.37361613949,4.16074084943798,337.622483297624));
#48056=CARTESIAN_POINT('Ctrl Pts',(176.365842469086,4.233854372873,337.506483922575));
#48057=CARTESIAN_POINT('Ctrl Pts',(176.358068798682,4.30203578467009,337.387547599383));
#48058=CARTESIAN_POINT('Ctrl Pts',(176.350295128277,4.36506481145655,337.266140387153));
#48059=CARTESIAN_POINT('Ctrl Pts',(176.342883324096,4.42515982192092,337.150384709786));
#48060=CARTESIAN_POINT('Ctrl Pts',(176.335471519915,4.48057121702699,337.032383266751));
#48061=CARTESIAN_POINT('Ctrl Pts',(176.328059715733,4.53114976219593,336.912554546948));
#48062=CARTESIAN_POINT('Ctrl Pts',(176.320284636955,4.58420731249719,336.786852664712));
#48063=CARTESIAN_POINT('Ctrl Pts',(176.312509558176,4.63211396114196,336.658742614917));
#48064=CARTESIAN_POINT('Ctrl Pts',(176.304734479398,4.67464479772458,336.528685408319));
#48065=CARTESIAN_POINT('Ctrl Pts',(176.296968968349,4.71712329740518,336.398788245393));
#48066=CARTESIAN_POINT('Ctrl Pts',(176.2892034573,4.75423902720225,336.266949061178));
#48067=CARTESIAN_POINT('Ctrl Pts',(176.281437946251,4.78581447925148,336.13365022502));
#48068=CARTESIAN_POINT('Ctrl Pts',(176.273680134729,4.81735862414818,336.000483555045));
#48069=CARTESIAN_POINT('Ctrl Pts',(176.265922323207,4.84337333356298,335.865860491132));
#48070=CARTESIAN_POINT('Ctrl Pts',(176.258164511685,4.86373053050184,335.730279665035));
#48071=CARTESIAN_POINT('Ctrl Pts',(176.250412538162,4.88407240800433,335.594800867811));
#48072=CARTESIAN_POINT('Ctrl Pts',(176.242660564639,4.89876518948732,335.458366127998));
#48073=CARTESIAN_POINT('Ctrl Pts',(176.234908591116,4.90773169826503,335.321485054621));
#48074=CARTESIAN_POINT('Ctrl Pts',(176.227159900559,4.91669440972094,335.18466195046));
#48075=CARTESIAN_POINT('Ctrl Pts',(176.219411210001,4.91993564628801,335.047393277914));
#48076=CARTESIAN_POINT('Ctrl Pts',(176.211662519444,4.9174300206283,334.910194350269));
#48077=CARTESIAN_POINT('Ctrl Pts',(176.203915441066,4.91492491628493,334.773023968007));
#48078=CARTESIAN_POINT('Ctrl Pts',(176.196168362688,4.90667533514496,334.635923692346));
#48079=CARTESIAN_POINT('Ctrl Pts',(176.18842128431,4.89270801706991,334.499409027049));
#48080=CARTESIAN_POINT('Ctrl Pts',(176.180674141005,4.87874058193527,334.362893217628));
#48081=CARTESIAN_POINT('Ctrl Pts',(176.172926997699,4.8590553540693,334.226963417206));
#48082=CARTESIAN_POINT('Ctrl Pts',(176.165179854393,4.83373093657324,334.092129802607));
#48083=CARTESIAN_POINT('Ctrl Pts',(176.157430969365,4.80840082561055,333.957265874549));
#48084=CARTESIAN_POINT('Ctrl Pts',(176.149682084337,4.77742907435664,333.823499006796));
#48085=CARTESIAN_POINT('Ctrl Pts',(176.141933199309,4.74094528667819,333.691328593105));
#48086=CARTESIAN_POINT('Ctrl Pts',(176.134176089535,4.70442277473052,333.559017892372));
#48087=CARTESIAN_POINT('Ctrl Pts',(176.12641897976,4.66237664354093,333.428307407988));
#48088=CARTESIAN_POINT('Ctrl Pts',(176.118661869985,4.61498639547701,333.299681314558));
#48089=CARTESIAN_POINT('Ctrl Pts',(176.110900615059,4.56757082357981,333.170986487457));
#48090=CARTESIAN_POINT('Ctrl Pts',(176.103139360133,4.51480559480765,333.044378631334));
#48091=CARTESIAN_POINT('Ctrl Pts',(176.095378105207,4.45691777002193,332.920320444452));
#48092=CARTESIAN_POINT('Ctrl Pts',(176.087604434803,4.39893734358217,332.796063804903));
#48093=CARTESIAN_POINT('Ctrl Pts',(176.079830764398,4.33581812618019,332.674365332089));
#48094=CARTESIAN_POINT('Ctrl Pts',(176.072057093994,4.26783283429882,332.555662469915));
#48095=CARTESIAN_POINT('Ctrl Pts',(176.064645289815,4.20301227409989,332.442485254514));
#48096=CARTESIAN_POINT('Ctrl Pts',(176.057233485637,4.13376862862668,332.332031278521));
#48097=CARTESIAN_POINT('Ctrl Pts',(176.049821681459,4.06037305472955,332.224652504834));
#48098=CARTESIAN_POINT('Ctrl Pts',(176.04204660268,3.98338014513169,332.112010777597));
#48099=CARTESIAN_POINT('Ctrl Pts',(176.034271523902,3.90157470761217,332.002397355807));
#48100=CARTESIAN_POINT('Ctrl Pts',(176.026496445123,3.81522270402468,331.896250850794));
#48101=CARTESIAN_POINT('Ctrl Pts',(176.018730934074,3.72897696207507,331.790234965814));
#48102=CARTESIAN_POINT('Ctrl Pts',(176.010965423025,3.63819603049299,331.687677809286));
#48103=CARTESIAN_POINT('Ctrl Pts',(176.003199911976,3.54318948426011,331.588989689091));
#48104=CARTESIAN_POINT('Ctrl Pts',(175.995442100453,3.44827713729456,331.490399418455));
#48105=CARTESIAN_POINT('Ctrl Pts',(175.987684288931,3.34914778277772,331.395670829754));
#48106=CARTESIAN_POINT('Ctrl Pts',(175.979926477409,3.24615142097872,331.305181463918));
#48107=CARTESIAN_POINT('Ctrl Pts',(175.972174503885,3.14323256720816,331.214760194199));
#48108=CARTESIAN_POINT('Ctrl Pts',(175.964422530362,3.03645279091959,331.128572054455));
#48109=CARTESIAN_POINT('Ctrl Pts',(175.956670556839,2.92619886848063,331.046957722892));
#48110=CARTESIAN_POINT('Ctrl Pts',(175.948921866281,2.815991638643,330.965377955047));
#48111=CARTESIAN_POINT('Ctrl Pts',(175.941173175723,2.70231350248418,330.888368374878));
#48112=CARTESIAN_POINT('Ctrl Pts',(175.933424485166,2.58558405939438,330.816229196729));
#48113=CARTESIAN_POINT('Ctrl Pts',(175.925677406788,2.46887890284024,330.744105027737));
#48114=CARTESIAN_POINT('Ctrl Pts',(175.91793032841,2.34912403440981,330.676849450542));
#48115=CARTESIAN_POINT('Ctrl Pts',(175.910183250032,2.22676742268942,330.61471894769));
#48116=CARTESIAN_POINT('Ctrl Pts',(175.902436106726,2.10440978550293,330.552587924124));
#48117=CARTESIAN_POINT('Ctrl Pts',(175.89468896342,1.97945071005153,330.495582237544));
#48118=CARTESIAN_POINT('Ctrl Pts',(175.886941820114,1.85236175155943,330.44391187488));
#48119=CARTESIAN_POINT('Ctrl Pts',(175.879192935085,1.72524422077117,330.392229895621));
#48120=CARTESIAN_POINT('Ctrl Pts',(175.871444050057,1.59599621611924,330.345885774323));
#48121=CARTESIAN_POINT('Ctrl Pts',(175.863695165029,1.46510782455742,330.305040774946));
#48122=CARTESIAN_POINT('Ctrl Pts',(175.855938055254,1.33408050670447,330.264152422265));
#48123=CARTESIAN_POINT('Ctrl Pts',(175.848180945479,1.20140969760162,330.228774967733));
#48124=CARTESIAN_POINT('Ctrl Pts',(175.840423835704,1.0675996890353,330.199019478641));
#48125=CARTESIAN_POINT('Ctrl Pts',(175.832662580778,0.933718176678549,330.169248089166));
#48126=CARTESIAN_POINT('Ctrl Pts',(175.824901325852,0.798696636441872,330.145104720035));
#48127=CARTESIAN_POINT('Ctrl Pts',(175.817140070925,0.663047036828604,330.126648823504));
#48128=CARTESIAN_POINT('Ctrl Pts',(175.80936640052,0.527180442064314,330.108163403554));
#48129=CARTESIAN_POINT('Ctrl Pts',(175.801592730116,0.390684169631619,330.095383673364));
#48130=CARTESIAN_POINT('Ctrl Pts',(175.793819059711,0.254073657977923,330.088317025823));
#48131=CARTESIAN_POINT('Ctrl Pts',(175.786407255535,0.123822398544541,330.081579332426));
#48132=CARTESIAN_POINT('Ctrl Pts',(175.77899545136,-0.0065324160113929,
330.080034806898));
#48133=CARTESIAN_POINT('Ctrl Pts',(175.771583647185,-0.136548074050385,
330.083645894977));
#48134=CARTESIAN_POINT('Ctrl Pts',(175.763808568407,-0.272936186820303,
330.087433973241));
#48135=CARTESIAN_POINT('Ctrl Pts',(175.756033489628,-0.409382067935774,
330.096907798746));
#48136=CARTESIAN_POINT('Ctrl Pts',(175.74825841085,-0.545372952551393,330.112081076253));
#48137=CARTESIAN_POINT('Ctrl Pts',(175.740492899801,-0.681196491726141,
330.127235682076));
#48138=CARTESIAN_POINT('Ctrl Pts',(175.732727388752,-0.816565763695584,
330.148075742043));
#48139=CARTESIAN_POINT('Ctrl Pts',(175.724961877703,-0.950968203023476,
330.174562969084));
#48140=CARTESIAN_POINT('Ctrl Pts',(175.717204066181,-1.08523738194049,330.201023933962));
#48141=CARTESIAN_POINT('Ctrl Pts',(175.709446254659,-1.2185412548911,330.233120848133));
#48142=CARTESIAN_POINT('Ctrl Pts',(175.701688443137,-1.35037293442409,330.270763697966));
#48143=CARTESIAN_POINT('Ctrl Pts',(175.693936469614,-1.48210540643809,330.308378220361));
#48144=CARTESIAN_POINT('Ctrl Pts',(175.686184496091,-1.61236751586079,330.351530264396));
#48145=CARTESIAN_POINT('Ctrl Pts',(175.678432522568,-1.74066347223494,330.400078942098));
#48146=CARTESIAN_POINT('Ctrl Pts',(175.670683832011,-1.86890509519553,330.448607059407));
#48147=CARTESIAN_POINT('Ctrl Pts',(175.662935141453,-1.99518185640903,330.502527126678));
#48148=CARTESIAN_POINT('Ctrl Pts',(175.655186450896,-2.11901422992423,330.561648757041));
#48149=CARTESIAN_POINT('Ctrl Pts',(175.647439372518,-2.24282083908013,330.620758086654));
#48150=CARTESIAN_POINT('Ctrl Pts',(175.63969229414,-2.36418371961667,330.685066658427));
#48151=CARTESIAN_POINT('Ctrl Pts',(175.631945215762,-2.48264476838242,330.754336563442));
#48152=CARTESIAN_POINT('Ctrl Pts',(175.624198072457,-2.60110680996515,330.823607049005));
#48153=CARTESIAN_POINT('Ctrl Pts',(175.616450929151,-2.71666663384779,330.897838753439));
#48154=CARTESIAN_POINT('Ctrl Pts',(175.608703785845,-2.8288924719523,330.976748771872));
#48155=CARTESIAN_POINT('Ctrl Pts',(175.600954900817,-2.94114354080819,331.055676530953));
#48156=CARTESIAN_POINT('Ctrl Pts',(175.593206015789,-3.05005881268118,331.139284472186));
#48157=CARTESIAN_POINT('Ctrl Pts',(175.585457130761,-3.15523746309426,331.227247740179));
#48158=CARTESIAN_POINT('Ctrl Pts',(175.577700020986,-3.26052775121363,331.315304373293));
#48159=CARTESIAN_POINT('Ctrl Pts',(175.569942911212,-3.3620731949287,331.407725316465));
#48160=CARTESIAN_POINT('Ctrl Pts',(175.562185801437,-3.45950749416334,331.504146604858));
#48161=CARTESIAN_POINT('Ctrl Pts',(175.554424546511,-3.55699385917205,331.600619417704));
#48162=CARTESIAN_POINT('Ctrl Pts',(175.546663291585,-3.65036443630706,331.701096549058));
#48163=CARTESIAN_POINT('Ctrl Pts',(175.538902036659,-3.73929217536197,331.805179646713));
#48164=CARTESIAN_POINT('Ctrl Pts',(175.531128366254,-3.828362169818,331.909429243404));
#48165=CARTESIAN_POINT('Ctrl Pts',(175.52335469585,-3.91297488274637,332.017296025601));
#48166=CARTESIAN_POINT('Ctrl Pts',(175.515581025445,-3.99284516399051,332.128350550834));
#48167=CARTESIAN_POINT('Ctrl Pts',(175.508169221267,-4.06899746443525,332.23423546121));
#48168=CARTESIAN_POINT('Ctrl Pts',(175.500757417089,-4.14083875884401,332.343017774418));
#48169=CARTESIAN_POINT('Ctrl Pts',(175.493345612912,-4.20816105072475,332.454304882029));
#48170=CARTESIAN_POINT('Ctrl Pts',(175.485316210545,-4.28109305982305,332.574865132104));
#48171=CARTESIAN_POINT('Ctrl Pts',(175.477286808179,-4.34893939756361,332.698725310259));
#48172=CARTESIAN_POINT('Ctrl Pts',(175.469257405813,-4.41139899220035,332.825432918001));
#48173=CARTESIAN_POINT('Ctrl Pts',(175.461240024851,-4.47376507401649,332.951950822529));
#48174=CARTESIAN_POINT('Ctrl Pts',(175.453222643889,-4.53076031911879,333.081307349566));
#48175=CARTESIAN_POINT('Ctrl Pts',(175.445205262928,-4.58212772700723,333.213022508286));
#48176=CARTESIAN_POINT('Ctrl Pts',(175.437198648785,-4.63342615182149,333.34456078215));
#48177=CARTESIAN_POINT('Ctrl Pts',(175.429192034643,-4.67911166530576,333.478451048872));
#48178=CARTESIAN_POINT('Ctrl Pts',(175.4211854205,-4.71897386982171,333.6141902445));
#48179=CARTESIAN_POINT('Ctrl Pts',(175.413191135583,-4.75877469132224,333.749720418041));
#48180=CARTESIAN_POINT('Ctrl Pts',(175.405196850666,-4.79276998154569,333.887093504415));
#48181=CARTESIAN_POINT('Ctrl Pts',(175.397202565749,-4.82079818617205,334.025788569816));
#48182=CARTESIAN_POINT('Ctrl Pts',(175.389215601938,-4.84880072277973,334.164356619322));
#48183=CARTESIAN_POINT('Ctrl Pts',(175.381228638128,-4.87084698663245,334.304243889378));
#48184=CARTESIAN_POINT('Ctrl Pts',(175.373241674317,-4.88682560210799,334.444915684709));
#48185=CARTESIAN_POINT('Ctrl Pts',(175.365262388803,-4.90278885648177,334.585452244684));
#48186=CARTESIAN_POINT('Ctrl Pts',(175.35728310329,-4.91269604999984,334.726771473829));
#48187=CARTESIAN_POINT('Ctrl Pts',(175.349303817776,-4.91648717332359,334.868330196914));
#48188=CARTESIAN_POINT('Ctrl Pts',(175.346808337353,-4.91767282760537,334.91260195803));
#48189=CARTESIAN_POINT('Ctrl Pts',(175.344312856931,-4.91826065279927,334.956897091092));
#48190=CARTESIAN_POINT('Ctrl Pts',(175.341817376508,-4.9182498538837,335.001198863214));
#48191=CARTESIAN_POINT('',(173.591817376561,-4.918248352634,335.004025458105));
#48192=CARTESIAN_POINT('Ctrl Pts',(175.341817376454,-4.91824985388346,335.001198864178));
#48193=CARTESIAN_POINT('Ctrl Pts',(175.333534918477,-4.91821401243364,335.1482357083));
#48194=CARTESIAN_POINT('Ctrl Pts',(175.325252460499,-4.91158018368582,335.295096105342));
#48195=CARTESIAN_POINT('Ctrl Pts',(175.316970002522,-4.89842102387199,335.441196708271));
#48196=CARTESIAN_POINT('Ctrl Pts',(175.308481467198,-4.88493444860438,335.59093246693));
#48197=CARTESIAN_POINT('Ctrl Pts',(175.299992931875,-4.86459368168669,335.739869785143));
#48198=CARTESIAN_POINT('Ctrl Pts',(175.291504396551,-4.83753179226554,335.887394625474));
#48199=CARTESIAN_POINT('Ctrl Pts',(175.283178484465,-4.81098835413402,336.032093187028));
#48200=CARTESIAN_POINT('Ctrl Pts',(175.27485257238,-4.77797915311206,336.175432643527));
#48201=CARTESIAN_POINT('Ctrl Pts',(175.266526660294,-4.7386797945413,336.316851118125));
#48202=CARTESIAN_POINT('Ctrl Pts',(175.257956813351,-4.69822903257857,336.462412909999));
#48203=CARTESIAN_POINT('Ctrl Pts',(175.249386966408,-4.65111405515187,336.605939105334));
#48204=CARTESIAN_POINT('Ctrl Pts',(175.240817119466,-4.59757875988788,336.746840750935));
#48205=CARTESIAN_POINT('Ctrl Pts',(175.232247272523,-4.54404346462389,336.887742396536));
#48206=CARTESIAN_POINT('Ctrl Pts',(175.22367742558,-4.48408805384567,337.026019210004));
#48207=CARTESIAN_POINT('Ctrl Pts',(175.215107578637,-4.41800674350231,337.161110704445));
#48208=CARTESIAN_POINT('Ctrl Pts',(175.207332499859,-4.35805381818948,337.283673804882));
#48209=CARTESIAN_POINT('Ctrl Pts',(175.19955742108,-4.29290212467153,337.403933892506));
#48210=CARTESIAN_POINT('Ctrl Pts',(175.191782342302,-4.22275162680702,337.521418600867));
#48211=CARTESIAN_POINT('Ctrl Pts',(175.184016831253,-4.15268745359612,337.638758736815));
#48212=CARTESIAN_POINT('Ctrl Pts',(175.176251320204,-4.07763691392763,337.753329956538));
#48213=CARTESIAN_POINT('Ctrl Pts',(175.168485809155,-3.99784720897207,337.864681615156));
#48214=CARTESIAN_POINT('Ctrl Pts',(175.160727997633,-3.91813661574133,337.975922868281));
#48215=CARTESIAN_POINT('Ctrl Pts',(175.15297018611,-3.83369643449449,338.083950597289));
#48216=CARTESIAN_POINT('Ctrl Pts',(175.145212374588,-3.74481859252371,338.18834075525));
#48217=CARTESIAN_POINT('Ctrl Pts',(175.137460401065,-3.65600763394762,338.292652356307));
#48218=CARTESIAN_POINT('Ctrl Pts',(175.129708427542,-3.56276591409088,338.393331538536));
#48219=CARTESIAN_POINT('Ctrl Pts',(175.121956454019,-3.46542706564282,338.489985431948));
#48220=CARTESIAN_POINT('Ctrl Pts',(175.114207763461,-3.36812944025466,338.58659839238));
#48221=CARTESIAN_POINT('Ctrl Pts',(175.106459072904,-3.26673841412597,338.679189179708));
#48222=CARTESIAN_POINT('Ctrl Pts',(175.098710382346,-3.16162593260944,338.767400234213));
#48223=CARTESIAN_POINT('Ctrl Pts',(175.090963303968,-3.05653532062261,338.855592935672));
#48224=CARTESIAN_POINT('Ctrl Pts',(175.08321622559,-2.94772509256875,338.939407465718));
#48225=CARTESIAN_POINT('Ctrl Pts',(175.075469147212,-2.83560157018039,339.018525450671));
#48226=CARTESIAN_POINT('Ctrl Pts',(175.067722003907,-2.72347710808881,339.097644098709));
#48227=CARTESIAN_POINT('Ctrl Pts',(175.059974860601,-2.60803961564551,339.172065897786));
#48228=CARTESIAN_POINT('Ctrl Pts',(175.052227717295,-2.48972545671888,339.241515084574));
#48229=CARTESIAN_POINT('Ctrl Pts',(175.044478832267,-2.37138469825763,339.310979885013));
#48230=CARTESIAN_POINT('Ctrl Pts',(175.036729947239,-2.25016632340666,339.375469650738));
#48231=CARTESIAN_POINT('Ctrl Pts',(175.028981062211,-2.12653205709415,339.434754161467));
#48232=CARTESIAN_POINT('Ctrl Pts',(175.021223952436,-2.00276656409396,339.494101597389));
#48233=CARTESIAN_POINT('Ctrl Pts',(175.013466842661,-1.87658041030347,339.548232572515));
#48234=CARTESIAN_POINT('Ctrl Pts',(175.005709732886,-1.74845661241411,339.596964491597));
#48235=CARTESIAN_POINT('Ctrl Pts',(174.99794847796,-1.62026434926375,339.645722451459));
#48236=CARTESIAN_POINT('Ctrl Pts',(174.990187223034,-1.49013274950522,339.689075483008));
#48237=CARTESIAN_POINT('Ctrl Pts',(174.982425968108,-1.35855986608731,339.726890960532));
#48238=CARTESIAN_POINT('Ctrl Pts',(174.974652297703,-1.22677650893543,339.764766930496));
#48239=CARTESIAN_POINT('Ctrl Pts',(174.966878627298,-1.09354764094046,339.797087552765));
#48240=CARTESIAN_POINT('Ctrl Pts',(174.959104956894,-0.959382252510918,
339.823771217219));
#48241=CARTESIAN_POINT('Ctrl Pts',(174.951693152717,-0.831462295196669,
339.849212750671));
#48242=CARTESIAN_POINT('Ctrl Pts',(174.94428134854,-0.702691329622126,339.869530271913));
#48243=CARTESIAN_POINT('Ctrl Pts',(174.936869544363,-0.573512857440891,
339.884697131333));
#48244=CARTESIAN_POINT('Ctrl Pts',(174.929094465585,-0.438002963530012,
339.900607363713));
#48245=CARTESIAN_POINT('Ctrl Pts',(174.921319386806,-0.301616370445505,
339.910899548619));
#48246=CARTESIAN_POINT('Ctrl Pts',(174.913544308028,-0.164858513129928,
339.915486215335));
#48247=CARTESIAN_POINT('Ctrl Pts',(174.905778796979,-0.0282689450642106,
339.920067237865));
#48248=CARTESIAN_POINT('Ctrl Pts',(174.89801328593,0.108690591283536,339.918956699013));
#48249=CARTESIAN_POINT('Ctrl Pts',(174.890247774881,0.245507364282319,339.912118605712));
#48250=CARTESIAN_POINT('Ctrl Pts',(174.882489963359,0.382188483052412,339.905287292401));
#48251=CARTESIAN_POINT('Ctrl Pts',(174.874732151837,0.518726732294366,339.892739745334));
#48252=CARTESIAN_POINT('Ctrl Pts',(174.866974340314,0.654607543290001,339.874491976275));
#48253=CARTESIAN_POINT('Ctrl Pts',(174.859222366791,0.790386099666195,339.85625793924));
#48254=CARTESIAN_POINT('Ctrl Pts',(174.851470393268,0.925507816721279,339.832332270262));
#48255=CARTESIAN_POINT('Ctrl Pts',(174.843718419745,1.05946177390906,339.802782923694));
#48256=CARTESIAN_POINT('Ctrl Pts',(174.835969729188,1.19335900151648,339.773246091291));
#48257=CARTESIAN_POINT('Ctrl Pts',(174.82822103863,1.32608907197248,339.738090402219));
#48258=CARTESIAN_POINT('Ctrl Pts',(174.820472348073,1.45715002470735,339.697435137178));
#48259=CARTESIAN_POINT('Ctrl Pts',(174.812725269695,1.58818370911642,339.656788330804));
#48260=CARTESIAN_POINT('Ctrl Pts',(174.804978191317,1.71754859346586,339.610644340155));
#48261=CARTESIAN_POINT('Ctrl Pts',(174.797231112939,1.84475706653118,339.559172559575));
#48262=CARTESIAN_POINT('Ctrl Pts',(174.789483969634,1.97196660572588,339.507700347613));
#48263=CARTESIAN_POINT('Ctrl Pts',(174.781736826328,2.09701933525203,339.45090040327));
#48264=CARTESIAN_POINT('Ctrl Pts',(174.773989683022,2.21944721831459,339.388990442871));
#48265=CARTESIAN_POINT('Ctrl Pts',(174.766240797994,2.34190262576438,339.327066563799));
#48266=CARTESIAN_POINT('Ctrl Pts',(174.758491912966,2.4617316637317,339.260030558963));
#48267=CARTESIAN_POINT('Ctrl Pts',(174.750743027938,2.57849086921786,339.188146117301));
#48268=CARTESIAN_POINT('Ctrl Pts',(174.742985918163,2.69537400413122,339.116185376749));
#48269=CARTESIAN_POINT('Ctrl Pts',(174.735228808388,2.80918046432426,339.039366124639));
#48270=CARTESIAN_POINT('Ctrl Pts',(174.727471698614,2.91949531350993,338.957995727245));
#48271=CARTESIAN_POINT('Ctrl Pts',(174.719710443687,3.02986911142376,338.876581848113));
#48272=CARTESIAN_POINT('Ctrl Pts',(174.711949188761,3.13674727612849,338.790612222609));
#48273=CARTESIAN_POINT('Ctrl Pts',(174.704187933835,3.2397487548041,338.700433902699));
#48274=CARTESIAN_POINT('Ctrl Pts',(174.696414263431,3.34291500227752,338.610111326867));
#48275=CARTESIAN_POINT('Ctrl Pts',(174.688640593026,3.44219188821686,338.515566872724));
#48276=CARTESIAN_POINT('Ctrl Pts',(174.680866922621,3.53723534101436,338.417184397246));
#48277=CARTESIAN_POINT('Ctrl Pts',(174.673455118444,3.6278544982194,338.323381649669));
#48278=CARTESIAN_POINT('Ctrl Pts',(174.666043314267,3.71462529364057,338.226090374067));
#48279=CARTESIAN_POINT('Ctrl Pts',(174.65863151009,3.79728531285856,338.125669098809));
#48280=CARTESIAN_POINT('Ctrl Pts',(174.650856431311,3.88399674584863,338.020325877712));
#48281=CARTESIAN_POINT('Ctrl Pts',(174.643081352533,3.96645827508929,337.911205173725));
#48282=CARTESIAN_POINT('Ctrl Pts',(174.635306273754,4.04432282474056,337.79868468245));
#48283=CARTESIAN_POINT('Ctrl Pts',(174.627540762705,4.12209155710639,337.686302654803));
#48284=CARTESIAN_POINT('Ctrl Pts',(174.619775251656,4.19527434514702,337.570529482489));
#48285=CARTESIAN_POINT('Ctrl Pts',(174.612009740607,4.26356345302084,337.451776854562));
#48286=CARTESIAN_POINT('Ctrl Pts',(174.604251929085,4.33178485204538,337.333141970211));
#48287=CARTESIAN_POINT('Ctrl Pts',(174.596494117563,4.39512203325476,337.211533845812));
#48288=CARTESIAN_POINT('Ctrl Pts',(174.588736306041,4.45330999862246,337.087393858061));
#48289=CARTESIAN_POINT('Ctrl Pts',(174.580984332518,4.51145417570094,336.963347289587));
#48290=CARTESIAN_POINT('Ctrl Pts',(174.573232358995,4.5644566846066,336.836773002681));
#48291=CARTESIAN_POINT('Ctrl Pts',(174.565480385472,4.61209818118046,336.70813741533));
#48292=CARTESIAN_POINT('Ctrl Pts',(174.557731694914,4.65971950155225,336.579556305227));
#48293=CARTESIAN_POINT('Ctrl Pts',(174.549983004356,4.70198418977133,336.448915996719));
#48294=CARTESIAN_POINT('Ctrl Pts',(174.542234313799,4.73872091185687,336.316703148789));
#48295=CARTESIAN_POINT('Ctrl Pts',(174.534487235421,4.77544999056055,336.184517808846));
#48296=CARTESIAN_POINT('Ctrl Pts',(174.526740157043,4.80665328626123,336.050760956636));
#48297=CARTESIAN_POINT('Ctrl Pts',(174.518993078665,4.83220937186604,335.91593430384));
#48298=CARTESIAN_POINT('Ctrl Pts',(174.511245935359,4.85776567165545,335.781106521066));
#48299=CARTESIAN_POINT('Ctrl Pts',(174.503498792054,4.87767459415442,335.645209303861));
#48300=CARTESIAN_POINT('Ctrl Pts',(174.495751648748,4.89186594009986,335.508754053144));
#48301=CARTESIAN_POINT('Ctrl Pts',(174.48800276372,4.90606047656115,335.372268124391));
#48302=CARTESIAN_POINT('Ctrl Pts',(174.480253878692,4.91453483817671,335.235224301182));
#48303=CARTESIAN_POINT('Ctrl Pts',(174.472504993664,4.91727078332571,335.098138198228));
#48304=CARTESIAN_POINT('Ctrl Pts',(174.464747883889,4.92000963243516,334.960906590668));
#48305=CARTESIAN_POINT('Ctrl Pts',(174.456990774114,4.91699789029285,334.823633005133));
#48306=CARTESIAN_POINT('Ctrl Pts',(174.449233664339,4.9082694819223,334.686832703926));
#48307=CARTESIAN_POINT('Ctrl Pts',(174.441472409413,4.8995364093694,334.549959301013));
#48308=CARTESIAN_POINT('Ctrl Pts',(174.433711154487,4.88508062479064,334.41356007487));
#48309=CARTESIAN_POINT('Ctrl Pts',(174.425949899561,4.86498776204339,334.278143270678));
#48310=CARTESIAN_POINT('Ctrl Pts',(174.418176229156,4.84486275726399,334.142509843731));
#48311=CARTESIAN_POINT('Ctrl Pts',(174.410402558751,4.81908272824628,334.007862363268));
#48312=CARTESIAN_POINT('Ctrl Pts',(174.402628888347,4.78778427161921,333.874697893481));
#48313=CARTESIAN_POINT('Ctrl Pts',(174.39521708417,4.7579427656778,333.747732261799));
#48314=CARTESIAN_POINT('Ctrl Pts',(174.387805279993,4.72308511271564,333.622114956956));
#48315=CARTESIAN_POINT('Ctrl Pts',(174.380393475815,4.68337079938713,333.498260669108));
#48316=CARTESIAN_POINT('Ctrl Pts',(174.372618397037,4.64170996925989,333.368335913671));
#48317=CARTESIAN_POINT('Ctrl Pts',(174.364843318258,4.59457270640252,333.239940780221));
#48318=CARTESIAN_POINT('Ctrl Pts',(174.35706823948,4.54208880045317,333.113571524998));
#48319=CARTESIAN_POINT('Ctrl Pts',(174.349302728431,4.48966947929138,332.987357775189));
#48320=CARTESIAN_POINT('Ctrl Pts',(174.341537217382,4.43191675461598,332.863165300837));
#48321=CARTESIAN_POINT('Ctrl Pts',(174.333771706333,4.36901029101437,332.741475672146));
#48322=CARTESIAN_POINT('Ctrl Pts',(174.326013894811,4.30616619935458,332.619906699075));
#48323=CARTESIAN_POINT('Ctrl Pts',(174.318256083289,4.23817871619064,332.500835978172));
#48324=CARTESIAN_POINT('Ctrl Pts',(174.310498271766,4.16527559896525,332.384725206185));
#48325=CARTESIAN_POINT('Ctrl Pts',(174.302746298243,4.0924273436475,332.268701811236));
#48326=CARTESIAN_POINT('Ctrl Pts',(174.29499432472,4.0146710242965,332.155634261263));
#48327=CARTESIAN_POINT('Ctrl Pts',(174.287242351197,3.93228016203768,332.045959412983));
#48328=CARTESIAN_POINT('Ctrl Pts',(174.27949366064,3.84992419235792,331.936331012066));
#48329=CARTESIAN_POINT('Ctrl Pts',(174.271744970082,3.76293781778694,331.830092766992));
#48330=CARTESIAN_POINT('Ctrl Pts',(174.263996279525,3.67163756159811,331.72765211526));
#48331=CARTESIAN_POINT('Ctrl Pts',(174.256249201147,3.58035630119013,331.625232777161));
#48332=CARTESIAN_POINT('Ctrl Pts',(174.248502122769,3.4847632043372,331.526609752416));
#48333=CARTESIAN_POINT('Ctrl Pts',(174.240755044391,3.38521445992893,331.432156656636));
#48334=CARTESIAN_POINT('Ctrl Pts',(174.233007901085,3.28566488120637,331.337702769248));
#48335=CARTESIAN_POINT('Ctrl Pts',(174.225260757779,3.18215987235577,331.24741914957));
#48336=CARTESIAN_POINT('Ctrl Pts',(174.217513614474,3.07509149247358,331.161641578042));
#48337=CARTESIAN_POINT('Ctrl Pts',(174.209764729446,2.96799904134648,331.075844721895));
#48338=CARTESIAN_POINT('Ctrl Pts',(174.202015844417,2.85734193003668,330.994556174108));
#48339=CARTESIAN_POINT('Ctrl Pts',(174.194266959389,2.74354387836738,330.918070303157));
#48340=CARTESIAN_POINT('Ctrl Pts',(174.186509849615,2.62962504027024,330.841503249311));
#48341=CARTESIAN_POINT('Ctrl Pts',(174.17875273984,2.51255892710305,330.769749273641));
#48342=CARTESIAN_POINT('Ctrl Pts',(174.170995630065,2.39279719270655,330.70305868587));
#48343=CARTESIAN_POINT('Ctrl Pts',(174.163234375139,2.27297146146842,330.636332460781));
#48344=CARTESIAN_POINT('Ctrl Pts',(174.155473120213,2.15044758774672,330.574675190583));
#48345=CARTESIAN_POINT('Ctrl Pts',(174.147711865287,2.02569930714924,330.518289904566));
#48346=CARTESIAN_POINT('Ctrl Pts',(174.139938194882,1.90075146995822,330.461814420468));
#48347=CARTESIAN_POINT('Ctrl Pts',(174.132164524477,1.77357247810012,330.410627919113));
#48348=CARTESIAN_POINT('Ctrl Pts',(174.124390854073,1.6446542437304,330.364884523436));
#48349=CARTESIAN_POINT('Ctrl Pts',(174.116979049896,1.52173718418788,330.321270493834));
#48350=CARTESIAN_POINT('Ctrl Pts',(174.109567245719,1.39723943647048,330.282604306296));
#48351=CARTESIAN_POINT('Ctrl Pts',(174.102155441542,1.27159602975758,330.248976257731));
#48352=CARTESIAN_POINT('Ctrl Pts',(174.094380362763,1.13979446540783,330.213699998332));
#48353=CARTESIAN_POINT('Ctrl Pts',(174.086605283985,1.00631558083169,330.183856754277));
#48354=CARTESIAN_POINT('Ctrl Pts',(174.078830205206,0.871646925110187,330.159605935417));
#48355=CARTESIAN_POINT('Ctrl Pts',(174.071064694157,0.737143987743028,330.135384958735));
#48356=CARTESIAN_POINT('Ctrl Pts',(174.063299183108,0.601454573357376,330.11674278298));
#48357=CARTESIAN_POINT('Ctrl Pts',(174.055533672059,0.465080871429679,330.103788929639));
#48358=CARTESIAN_POINT('Ctrl Pts',(174.047775860537,0.328842384424646,330.090847920081));
#48359=CARTESIAN_POINT('Ctrl Pts',(174.040018049015,0.191921346693514,330.083584045765));
#48360=CARTESIAN_POINT('Ctrl Pts',(174.032260237493,0.0548292615047352,
330.082055631203));
#48361=CARTESIAN_POINT('Ctrl Pts',(174.02450826397,-0.0821596575426619,
330.080528366821));
#48362=CARTESIAN_POINT('Ctrl Pts',(174.016756290447,-0.219318978563306,
330.084727975516));
#48363=CARTESIAN_POINT('Ctrl Pts',(174.009004316924,-0.356133321447015,
330.094660855776));
#48364=CARTESIAN_POINT('Ctrl Pts',(174.001255626366,-0.492889723375285,
330.104589529455));
#48365=CARTESIAN_POINT('Ctrl Pts',(173.993506935808,-0.629301048709266,
330.120246617246));
#48366=CARTESIAN_POINT('Ctrl Pts',(173.985758245251,-0.764853385657481,
330.141586435785));
#48367=CARTESIAN_POINT('Ctrl Pts',(173.978011166873,-0.900377519809782,
330.162921814397));
#48368=CARTESIAN_POINT('Ctrl Pts',(173.970264088495,-1.03504263518604,330.189937511252));
#48369=CARTESIAN_POINT('Ctrl Pts',(173.962517010117,-1.16834179620082,330.22253618436));
#48370=CARTESIAN_POINT('Ctrl Pts',(173.954769866811,-1.30164207439094,330.255135130676));
#48371=CARTESIAN_POINT('Ctrl Pts',(173.947022723505,-1.43357599570025,330.29331705372));
#48372=CARTESIAN_POINT('Ctrl Pts',(173.9392755802,-1.56364902951877,330.336933972697));
#48373=CARTESIAN_POINT('Ctrl Pts',(173.931526695172,-1.69375130651686,330.380560697684));
#48374=CARTESIAN_POINT('Ctrl Pts',(173.923777810143,-1.82199149299923,330.429624725807));
#48375=CARTESIAN_POINT('Ctrl Pts',(173.916028925115,-1.94789274912631,330.4839290417));
#48376=CARTESIAN_POINT('Ctrl Pts',(173.908271815341,-2.07392763814745,330.538290996755));
#48377=CARTESIAN_POINT('Ctrl Pts',(173.900514705566,-2.19761827817883,330.597904195336));
#48378=CARTESIAN_POINT('Ctrl Pts',(173.892757595791,-2.31850976262574,330.662524289047));
#48379=CARTESIAN_POINT('Ctrl Pts',(173.884996340865,-2.43946584761647,330.727178913669));
#48380=CARTESIAN_POINT('Ctrl Pts',(173.877235085939,-2.55761946001583,330.796845566216));
#48381=CARTESIAN_POINT('Ctrl Pts',(173.869473831012,-2.67254350264052,330.871235743107));
#48382=CARTESIAN_POINT('Ctrl Pts',(173.861700160608,-2.78765138627982,330.945744920038));
#48383=CARTESIAN_POINT('Ctrl Pts',(173.853926490203,-2.89951905730874,331.024992494573));
#48384=CARTESIAN_POINT('Ctrl Pts',(173.846152819798,-3.00775070856979,331.108648212048));
#48385=CARTESIAN_POINT('Ctrl Pts',(173.838741015621,-3.11094415042489,331.188409735748));
#48386=CARTESIAN_POINT('Ctrl Pts',(173.831329211444,-3.21083224740198,331.272178055105));
#48387=CARTESIAN_POINT('Ctrl Pts',(173.823917407267,-3.30710364765362,331.359636209638));
#48388=CARTESIAN_POINT('Ctrl Pts',(173.816258284257,-3.40658745473968,331.450012688541));
#48389=CARTESIAN_POINT('Ctrl Pts',(173.808599161247,-3.50254359561381,331.544633845094));
#48390=CARTESIAN_POINT('Ctrl Pts',(173.800940038236,-3.59457987923933,331.643189228707));
#48391=CARTESIAN_POINT('Ctrl Pts',(173.793290431619,-3.68650180859247,331.741622158123));
#48392=CARTESIAN_POINT('Ctrl Pts',(173.785640825001,-3.77451329351233,331.843979301775));
#48393=CARTESIAN_POINT('Ctrl Pts',(173.777991218384,-3.85825565553903,331.949910434266));
#48394=CARTESIAN_POINT('Ctrl Pts',(173.770233974975,-3.94317634733348,332.057332112327));
#48395=CARTESIAN_POINT('Ctrl Pts',(173.762476731565,-4.0237065286861,332.168428867022));
#48396=CARTESIAN_POINT('Ctrl Pts',(173.754719488156,-4.09951075861579,332.28279654746));
#48397=CARTESIAN_POINT('Ctrl Pts',(173.747083300453,-4.17413202520065,332.395379462406));
#48398=CARTESIAN_POINT('Ctrl Pts',(173.73944711275,-4.24417353419884,332.511131608632));
#48399=CARTESIAN_POINT('Ctrl Pts',(173.731810925048,-4.30935630741304,332.629634779563));
#48400=CARTESIAN_POINT('Ctrl Pts',(173.724177742638,-4.37451342733966,332.748091312466));
#48401=CARTESIAN_POINT('Ctrl Pts',(173.716544560228,-4.43481541967576,332.869296364216));
#48402=CARTESIAN_POINT('Ctrl Pts',(173.708911377818,-4.4900278589622,332.992804720949));
#48403=CARTESIAN_POINT('Ctrl Pts',(173.701279432926,-4.5452313470147,333.116293054075));
#48404=CARTESIAN_POINT('Ctrl Pts',(173.693647488034,-4.59534675937607,333.242083580868));
#48405=CARTESIAN_POINT('Ctrl Pts',(173.686015543143,-4.64018691907406,333.369709100021));
#48406=CARTESIAN_POINT('Ctrl Pts',(173.678165695928,-4.68630732582814,333.500978499933));
#48407=CARTESIAN_POINT('Ctrl Pts',(173.670315848712,-4.72684655661679,333.63418883275));
#48408=CARTESIAN_POINT('Ctrl Pts',(173.662466001497,-4.7616554662562,333.768813465322));
#48409=CARTESIAN_POINT('Ctrl Pts',(173.654828191045,-4.79552413230764,333.899801674092));
#48410=CARTESIAN_POINT('Ctrl Pts',(173.647190380592,-4.8239680256956,334.032128345781));
#48411=CARTESIAN_POINT('Ctrl Pts',(173.63955257014,-4.84690157851197,334.165297567562));
#48412=CARTESIAN_POINT('Ctrl Pts',(173.631596704543,-4.87079013466174,334.304012247202));
#48413=CARTESIAN_POINT('Ctrl Pts',(173.623640838947,-4.88869944154812,334.44364067942));
#48414=CARTESIAN_POINT('Ctrl Pts',(173.615684973351,-4.90059265648145,334.583617150041));
#48415=CARTESIAN_POINT('Ctrl Pts',(173.607729107754,-4.91248587141478,334.723593620662));
#48416=CARTESIAN_POINT('Ctrl Pts',(173.599773242158,-4.91836302723345,334.863917638052));
#48417=CARTESIAN_POINT('Ctrl Pts',(173.591817376561,-4.918248352634,335.004025458105));
#48418=CARTESIAN_POINT('',(171.841817376472,-4.91824887853913,334.996678667656));
#48419=CARTESIAN_POINT('Ctrl Pts',(173.591817376508,-4.91824835263323,335.004025459041));
#48420=CARTESIAN_POINT('Ctrl Pts',(173.579434926919,-4.91806987390456,335.222088220135));
#48421=CARTESIAN_POINT('Ctrl Pts',(173.567052477329,-4.90338612536152,335.439575567829));
#48422=CARTESIAN_POINT('Ctrl Pts',(173.55467002774,-4.87444124616087,335.654985190845));
#48423=CARTESIAN_POINT('Ctrl Pts',(173.551673142825,-4.86743580905111,335.70712009721));
#48424=CARTESIAN_POINT('Ctrl Pts',(173.548676257909,-4.85959517048378,335.759133471016));
#48425=CARTESIAN_POINT('Ctrl Pts',(173.545679372993,-4.85092312038314,335.81100428028));
#48426=CARTESIAN_POINT('Ctrl Pts',(173.537904294215,-4.82842446774871,335.945577225079));
#48427=CARTESIAN_POINT('Ctrl Pts',(173.530129215437,-4.80028609261384,336.079425884722));
#48428=CARTESIAN_POINT('Ctrl Pts',(173.522354136658,-4.7665648997525,336.212040477438));
#48429=CARTESIAN_POINT('Ctrl Pts',(173.514588625609,-4.73288520296578,336.344491879455));
#48430=CARTESIAN_POINT('Ctrl Pts',(173.50682311456,-4.69363645321306,336.475711860921));
#48431=CARTESIAN_POINT('Ctrl Pts',(173.499057603511,-4.64892702622161,336.605197983853));
#48432=CARTESIAN_POINT('Ctrl Pts',(173.491299791989,-4.60426192875721,336.734555720917));
#48433=CARTESIAN_POINT('Ctrl Pts',(173.483541980467,-4.55414705552233,336.862182653514));
#48434=CARTESIAN_POINT('Ctrl Pts',(173.475784168945,-4.49874123741858,336.987589077563));
#48435=CARTESIAN_POINT('Ctrl Pts',(173.468032195422,-4.44337711394991,337.112901129302));
#48436=CARTESIAN_POINT('Ctrl Pts',(173.460280221899,-4.38273012812621,337.235995642447));
#48437=CARTESIAN_POINT('Ctrl Pts',(173.452528248376,-4.31700797704738,337.35640089726));
#48438=CARTESIAN_POINT('Ctrl Pts',(173.444779557818,-4.25131365933858,337.476755160376));
#48439=CARTESIAN_POINT('Ctrl Pts',(173.43703086726,-4.18054863813499,337.594422087979));
#48440=CARTESIAN_POINT('Ctrl Pts',(173.429282176703,-4.10496740407348,337.708952874081));
#48441=CARTESIAN_POINT('Ctrl Pts',(173.421535098325,-4.02940189531899,337.823459831097));
#48442=CARTESIAN_POINT('Ctrl Pts',(173.413788019947,-3.94902238201836,337.934831618447));
#48443=CARTESIAN_POINT('Ctrl Pts',(173.406040941569,-3.86412748124862,338.042647181511));
#48444=CARTESIAN_POINT('Ctrl Pts',(173.398293798263,-3.7792318689779,338.150463648174));
#48445=CARTESIAN_POINT('Ctrl Pts',(173.390546654958,-3.68982103556894,338.254723524006));
#48446=CARTESIAN_POINT('Ctrl Pts',(173.382799511652,-3.59623454723086,338.355038024196));
#48447=CARTESIAN_POINT('Ctrl Pts',(173.375050626624,-3.50262701866331,338.455375077216));
#48448=CARTESIAN_POINT('Ctrl Pts',(173.367301741596,-3.40484223369459,338.551764703801));
#48449=CARTESIAN_POINT('Ctrl Pts',(173.359552856568,-3.30325705769649,338.643854535142));
#48450=CARTESIAN_POINT('Ctrl Pts',(173.351795746793,-3.20156405814299,338.736042111582));
#48451=CARTESIAN_POINT('Ctrl Pts',(173.344038637018,-3.09606289976757,338.823920513126));
#48452=CARTESIAN_POINT('Ctrl Pts',(173.336281527243,-2.98716444081456,338.907176943272));
#48453=CARTESIAN_POINT('Ctrl Pts',(173.328520272317,-2.87820779000694,338.990477862991));
#48454=CARTESIAN_POINT('Ctrl Pts',(173.320759017391,-2.76585054127866,339.069151665864));
#48455=CARTESIAN_POINT('Ctrl Pts',(173.312997762465,-2.65053221897531,339.142929159263));
#48456=CARTESIAN_POINT('Ctrl Pts',(173.30522409206,-2.5350294249385,339.216824672608));
#48457=CARTESIAN_POINT('Ctrl Pts',(173.297450421656,-2.41655642985469,339.285808028042));
#48458=CARTESIAN_POINT('Ctrl Pts',(173.289676751251,-2.29557779408966,339.349655808657));
#48459=CARTESIAN_POINT('Ctrl Pts',(173.282264947074,-2.18023074292691,339.410531459722));
#48460=CARTESIAN_POINT('Ctrl Pts',(173.274853142897,-2.0626063361906,339.466738774062));
#48461=CARTESIAN_POINT('Ctrl Pts',(173.26744133872,-1.94312204504458,339.518125693312));
#48462=CARTESIAN_POINT('Ctrl Pts',(173.259666259941,-1.81778147286245,339.572031238548));
#48463=CARTESIAN_POINT('Ctrl Pts',(173.251891181163,-1.68999799006784,339.620802268559));
#48464=CARTESIAN_POINT('Ctrl Pts',(173.244116102385,-1.56023107746598,339.664210763614));
#48465=CARTESIAN_POINT('Ctrl Pts',(173.236350591336,-1.43062385131145,339.707565841752));
#48466=CARTESIAN_POINT('Ctrl Pts',(173.228585080287,-1.29903841885686,339.745571392122));
#48467=CARTESIAN_POINT('Ctrl Pts',(173.220819569238,-1.1659559392467,339.778046652162));
#48468=CARTESIAN_POINT('Ctrl Pts',(173.213061757715,-1.03300541130252,339.810489712887));
#48469=CARTESIAN_POINT('Ctrl Pts',(173.205303946193,-0.898561167382252,
339.83741330329));
#48470=CARTESIAN_POINT('Ctrl Pts',(173.197546134671,-0.76312096260956,339.858685980687));
#48471=CARTESIAN_POINT('Ctrl Pts',(173.189794161148,-0.627782680886049,
339.87994264972));
#48472=CARTESIAN_POINT('Ctrl Pts',(173.182042187625,-0.491450314723244,
339.895556809719));
#48473=CARTESIAN_POINT('Ctrl Pts',(173.174290214102,-0.354632940132807,
339.905447842988));
#48474=CARTESIAN_POINT('Ctrl Pts',(173.166541523544,-0.21787350778175,339.915334687398));
#48475=CARTESIAN_POINT('Ctrl Pts',(173.158792832987,-0.0806298645773756,
339.919503197615));
#48476=CARTESIAN_POINT('Ctrl Pts',(173.151044142429,0.0565828594638976,
339.917924505573));
#48477=CARTESIAN_POINT('Ctrl Pts',(173.143297064051,0.193767035251864,339.916346141991));
#48478=CARTESIAN_POINT('Ctrl Pts',(173.135549985673,0.330919914069369,339.909022959081));
#48479=CARTESIAN_POINT('Ctrl Pts',(173.127802907296,0.467525823269463,339.895978213501));
#48480=CARTESIAN_POINT('Ctrl Pts',(173.12005576399,0.60413287735857,339.882933358593));
#48481=CARTESIAN_POINT('Ctrl Pts',(173.112308620684,0.740192563582616,339.864166882526));
#48482=CARTESIAN_POINT('Ctrl Pts',(173.104561477378,0.87519418573948,339.83975394));
#48483=CARTESIAN_POINT('Ctrl Pts',(173.09681259235,1.01022615912722,339.815335508927));
#48484=CARTESIAN_POINT('Ctrl Pts',(173.089063707322,1.14419921054186,339.785268154881));
#48485=CARTESIAN_POINT('Ctrl Pts',(173.081314822294,1.2766130820557,339.749678105011));
#48486=CARTESIAN_POINT('Ctrl Pts',(173.073557712519,1.40916749902087,339.714050279495));
#48487=CARTESIAN_POINT('Ctrl Pts',(173.065800602744,1.54015905213462,339.672888150186));
#48488=CARTESIAN_POINT('Ctrl Pts',(173.05804349297,1.66910236517373,339.626367944411));
#48489=CARTESIAN_POINT('Ctrl Pts',(173.050282238044,1.79811458139649,339.579822879725));
#48490=CARTESIAN_POINT('Ctrl Pts',(173.042520983117,1.92507601500787,339.527914181269));
#48491=CARTESIAN_POINT('Ctrl Pts',(173.034759728191,2.04952244434366,339.470865778866));
#48492=CARTESIAN_POINT('Ctrl Pts',(173.026986057787,2.17416794740941,339.413726117611));
#48493=CARTESIAN_POINT('Ctrl Pts',(173.019212387382,2.29629005830769,339.351430500424));
#48494=CARTESIAN_POINT('Ctrl Pts',(173.011438716977,2.41544950072452,339.284248682319));
#48495=CARTESIAN_POINT('Ctrl Pts',(173.0040269128,2.52906204242842,339.22019419401));
#48496=CARTESIAN_POINT('Ctrl Pts',(172.996615108623,2.63998128796015,339.151698323942));
#48497=CARTESIAN_POINT('Ctrl Pts',(172.989203304446,2.74785345059655,339.079029845018));
#48498=CARTESIAN_POINT('Ctrl Pts',(172.981428225668,2.86101274925862,339.002799667473));
#48499=CARTESIAN_POINT('Ctrl Pts',(172.973653146889,2.97117632363346,338.92173661347));
#48500=CARTESIAN_POINT('Ctrl Pts',(172.965878068111,3.07790377563761,338.83610367566));
#48501=CARTESIAN_POINT('Ctrl Pts',(172.958112557062,3.18449989271749,338.750576114633));
#48502=CARTESIAN_POINT('Ctrl Pts',(172.950347046013,3.28766799870819,338.660490101293));
#48503=CARTESIAN_POINT('Ctrl Pts',(172.942581534964,3.38699570369304,338.566152431636));
#48504=CARTESIAN_POINT('Ctrl Pts',(172.934823723441,3.48622492496919,338.471908298054));
#48505=CARTESIAN_POINT('Ctrl Pts',(172.927065911919,3.58162104132301,338.373421164741));
#48506=CARTESIAN_POINT('Ctrl Pts',(172.919308100397,3.67280415593889,338.271038473424));
#48507=CARTESIAN_POINT('Ctrl Pts',(172.911556126874,3.76391865236943,338.168732828328));
#48508=CARTESIAN_POINT('Ctrl Pts',(172.903804153351,3.85082619870627,338.062537751014));
#48509=CARTESIAN_POINT('Ctrl Pts',(172.896052179828,3.93318351156793,337.952837707499));
#48510=CARTESIAN_POINT('Ctrl Pts',(172.88830348927,4.01550594605869,337.843184122018));
#48511=CARTESIAN_POINT('Ctrl Pts',(172.880554798713,4.09328174560817,337.730028834551));
#48512=CARTESIAN_POINT('Ctrl Pts',(172.872806108155,4.16620786803315,337.61378940675));
#48513=CARTESIAN_POINT('Ctrl Pts',(172.865059029777,4.23911881756926,337.497574163533));
#48514=CARTESIAN_POINT('Ctrl Pts',(172.8573119514,4.30718188938616,337.378276387231));
#48515=CARTESIAN_POINT('Ctrl Pts',(172.849564873022,4.37013758044379,337.256342303484));
#48516=CARTESIAN_POINT('Ctrl Pts',(172.841817729716,4.43309379913072,337.134407197813));
#48517=CARTESIAN_POINT('Ctrl Pts',(172.83407058641,4.49094237235991,337.009836087941));
#48518=CARTESIAN_POINT('Ctrl Pts',(172.826323443104,4.5434701323031,336.883099099721));
#48519=CARTESIAN_POINT('Ctrl Pts',(172.818574558076,4.59600970160189,336.756333618335));
#48520=CARTESIAN_POINT('Ctrl Pts',(172.810825673048,4.64322592761838,336.627401650672));
#48521=CARTESIAN_POINT('Ctrl Pts',(172.80307678802,4.68495423918542,336.49679218305));
#48522=CARTESIAN_POINT('Ctrl Pts',(172.795319678245,4.72672684161353,336.366044085188));
#48523=CARTESIAN_POINT('Ctrl Pts',(172.787562568471,4.76299977460549,336.233615303541));
#48524=CARTESIAN_POINT('Ctrl Pts',(172.779805458696,4.79365856655512,336.100009368048));
#48525=CARTESIAN_POINT('Ctrl Pts',(172.77204420377,4.82433374158287,335.966332037814));
#48526=CARTESIAN_POINT('Ctrl Pts',(172.764282948844,4.84938872640018,335.831476684432));
#48527=CARTESIAN_POINT('Ctrl Pts',(172.756521693917,4.86876061139355,335.695954863079));
#48528=CARTESIAN_POINT('Ctrl Pts',(172.748748023513,4.88816348508963,335.560216250977));
#48529=CARTESIAN_POINT('Ctrl Pts',(172.740974353108,4.90186505315065,335.423809429581));
#48530=CARTESIAN_POINT('Ctrl Pts',(172.733200682703,4.90985444070406,335.287249775628));
#48531=CARTESIAN_POINT('Ctrl Pts',(172.725788878526,4.91747192034477,335.157047006422));
#48532=CARTESIAN_POINT('Ctrl Pts',(172.718377074349,4.91989705021166,335.026705600909));
#48533=CARTESIAN_POINT('Ctrl Pts',(172.710965270172,4.91716439287622,334.896668514333));
#48534=CARTESIAN_POINT('Ctrl Pts',(172.703190191394,4.91429779986462,334.760257922784));
#48535=CARTESIAN_POINT('Ctrl Pts',(172.695415112615,4.90574597962765,334.623751152937));
#48536=CARTESIAN_POINT('Ctrl Pts',(172.687640033837,4.89149176362454,334.487660865351));
#48537=CARTESIAN_POINT('Ctrl Pts',(172.679874522788,4.87725508834169,334.351738045527));
#48538=CARTESIAN_POINT('Ctrl Pts',(172.672109011739,4.85733001975963,334.216231073252));
#48539=CARTESIAN_POINT('Ctrl Pts',(172.66434350069,4.83175138132911,334.081652760921));
#48540=CARTESIAN_POINT('Ctrl Pts',(172.656585689167,4.80619810419306,333.947207883378));
#48541=CARTESIAN_POINT('Ctrl Pts',(172.648827877645,4.77500248504693,333.813690214924));
#48542=CARTESIAN_POINT('Ctrl Pts',(172.641070066123,4.7382511110836,333.681607239547));
#48543=CARTESIAN_POINT('Ctrl Pts',(172.6333180926,4.70152739369465,333.549623660798));
#48544=CARTESIAN_POINT('Ctrl Pts',(172.625566119077,4.65925634768551,333.419073001185));
#48545=CARTESIAN_POINT('Ctrl Pts',(172.617814145554,4.61157550839723,333.290451991651));
#48546=CARTESIAN_POINT('Ctrl Pts',(172.610065454996,4.56391486197267,333.16188545319));
#48547=CARTESIAN_POINT('Ctrl Pts',(172.602316764439,4.51084911458962,333.035247305177));
#48548=CARTESIAN_POINT('Ctrl Pts',(172.594568073881,4.45256540923669,332.911018348819));
#48549=CARTESIAN_POINT('Ctrl Pts',(172.586820995503,4.39429383029547,332.786815239334));
#48550=CARTESIAN_POINT('Ctrl Pts',(172.579073917125,4.33080661871464,332.665020678119));
#48551=CARTESIAN_POINT('Ctrl Pts',(172.571326838748,4.26233858317063,332.546094365116));
#48552=CARTESIAN_POINT('Ctrl Pts',(172.563579695442,4.19386997379856,332.427167055396));
#48553=CARTESIAN_POINT('Ctrl Pts',(172.555832552136,4.12042065222392,332.311108380582));
#48554=CARTESIAN_POINT('Ctrl Pts',(172.54808540883,4.04227059996193,332.198352010123));
#48555=CARTESIAN_POINT('Ctrl Pts',(172.540336523802,3.96410297790908,332.085570289637));
#48556=CARTESIAN_POINT('Ctrl Pts',(172.532587638774,3.88123274482247,331.976092672049));
#48557=CARTESIAN_POINT('Ctrl Pts',(172.524838753746,3.79398204082652,331.870322167317));
#48558=CARTESIAN_POINT('Ctrl Pts',(172.517081643971,3.70663872803182,331.764439396679));
#48559=CARTESIAN_POINT('Ctrl Pts',(172.509324534196,3.61490590568282,331.662271900966));
#48560=CARTESIAN_POINT('Ctrl Pts',(172.501567424422,3.51914505569374,331.564188430736));
#48561=CARTESIAN_POINT('Ctrl Pts',(172.493806169496,3.42333303416829,331.466052547836));
#48562=CARTESIAN_POINT('Ctrl Pts',(172.486044914569,3.32348898043557,331.372005306865));
#48563=CARTESIAN_POINT('Ctrl Pts',(172.478283659643,3.22000902815658,331.282376441718));
#48564=CARTESIAN_POINT('Ctrl Pts',(172.470509989239,3.11636354167797,331.192604199597));
#48565=CARTESIAN_POINT('Ctrl Pts',(172.462736318834,3.00907084012689,331.107264700625));
#48566=CARTESIAN_POINT('Ctrl Pts',(172.454962648429,2.89855842978221,331.026645989641));
#48567=CARTESIAN_POINT('Ctrl Pts',(172.447550844252,2.79319039872712,330.949780099048));
#48568=CARTESIAN_POINT('Ctrl Pts',(172.440139040075,2.68489590704514,330.877205542095));
#48569=CARTESIAN_POINT('Ctrl Pts',(172.432727235898,2.57406614904068,330.809132962875));
#48570=CARTESIAN_POINT('Ctrl Pts',(172.42495215712,2.45780429445129,330.737723943769));
#48571=CARTESIAN_POINT('Ctrl Pts',(172.417177078341,2.33838495880929,330.671043705931));
#48572=CARTESIAN_POINT('Ctrl Pts',(172.409401999563,2.21622995843308,330.609384116796));
#48573=CARTESIAN_POINT('Ctrl Pts',(172.401636488514,2.0942252775616,330.547800403711));
#48574=CARTESIAN_POINT('Ctrl Pts',(172.393870977465,1.969491975751,330.491225220878));
#48575=CARTESIAN_POINT('Ctrl Pts',(172.386105466416,1.84248013285272,330.439906796726));
#48576=CARTESIAN_POINT('Ctrl Pts',(172.378347654893,1.71559422256641,330.388639254941));
#48577=CARTESIAN_POINT('Ctrl Pts',(172.370589843371,1.5864346271641,330.342618244968));
#48578=CARTESIAN_POINT('Ctrl Pts',(172.362832031849,1.45547495805827,330.302045582494));
#48579=CARTESIAN_POINT('Ctrl Pts',(172.355080058326,1.32461384025657,330.261503452235));
#48580=CARTESIAN_POINT('Ctrl Pts',(172.347328084803,1.19195571690451,330.226401623726));
#48581=CARTESIAN_POINT('Ctrl Pts',(172.33957611128,1.05799272791318,330.196893250178));
#48582=CARTESIAN_POINT('Ctrl Pts',(172.331827420722,0.924086472327158,330.167397373444));
#48583=CARTESIAN_POINT('Ctrl Pts',(172.324078730165,0.788876831135882,330.143490324142));
#48584=CARTESIAN_POINT('Ctrl Pts',(172.316330039607,0.65286939414139,330.12527491886));
#48585=CARTESIAN_POINT('Ctrl Pts',(172.308582961229,0.516890254630074,330.107063303446));
#48586=CARTESIAN_POINT('Ctrl Pts',(172.300835882851,0.38011403664952,330.09454102846));
#48587=CARTESIAN_POINT('Ctrl Pts',(172.293088804474,0.243054380136059,330.087759408295));
#48588=CARTESIAN_POINT('Ctrl Pts',(172.285341661168,0.105993574930804,330.080977731293));
#48589=CARTESIAN_POINT('Ctrl Pts',(172.277594517862,-0.0313502831487476,
330.07993682439));
#48590=CARTESIAN_POINT('Ctrl Pts',(172.269847374556,-0.168460998147874,
330.08463592858));
#48591=CARTESIAN_POINT('Ctrl Pts',(172.262098489528,-0.305602538546488,
330.089336089229));
#48592=CARTESIAN_POINT('Ctrl Pts',(172.2543496045,-0.442510440995069,330.099778815489));
#48593=CARTESIAN_POINT('Ctrl Pts',(172.246600719472,-0.578671477315011,
330.115911304671));
#48594=CARTESIAN_POINT('Ctrl Pts',(172.238843609697,-0.714977036365965,
330.132060917043));
#48595=CARTESIAN_POINT('Ctrl Pts',(172.231086499922,-0.850533756960454,
330.15391231009));
#48596=CARTESIAN_POINT('Ctrl Pts',(172.223329390148,-0.984835930281048,
330.181361058045));
#48597=CARTESIAN_POINT('Ctrl Pts',(172.215568135222,-1.11920987038891,330.208824473732));
#48598=CARTESIAN_POINT('Ctrl Pts',(172.207806880295,-1.25232754825694,330.241891110077));
#48599=CARTESIAN_POINT('Ctrl Pts',(172.200045625369,-1.38369731296345,330.280406287762));
#48600=CARTESIAN_POINT('Ctrl Pts',(172.192271954965,-1.51527722648011,330.318983077179));
#48601=CARTESIAN_POINT('Ctrl Pts',(172.18449828456,-1.64510326906748,330.36302569923));
#48602=CARTESIAN_POINT('Ctrl Pts',(172.176724614155,-1.77270186949735,330.412330532353));
#48603=CARTESIAN_POINT('Ctrl Pts',(172.169312809978,-1.89436072437896,330.459340213632));
#48604=CARTESIAN_POINT('Ctrl Pts',(172.161901005801,-2.01399458101779,330.511133104955));
#48605=CARTESIAN_POINT('Ctrl Pts',(172.154489201624,-2.13121460661563,330.56749423429));
#48606=CARTESIAN_POINT('Ctrl Pts',(172.146714122846,-2.25417993484834,330.626617790466));
#48607=CARTESIAN_POINT('Ctrl Pts',(172.138939044067,-2.37487742420324,330.690955554701));
#48608=CARTESIAN_POINT('Ctrl Pts',(172.131163965289,-2.4928333681122,330.760310758873));
#48609=CARTESIAN_POINT('Ctrl Pts',(172.12339845424,-2.61064415972271,330.829580617051));
#48610=CARTESIAN_POINT('Ctrl Pts',(172.115632943191,-2.72571978475079,330.903855433897));
#48611=CARTESIAN_POINT('Ctrl Pts',(172.107867432142,-2.83760793858081,330.98289105831));
#48612=CARTESIAN_POINT('Ctrl Pts',(172.100109620619,-2.94938515498055,331.061848318672));
#48613=CARTESIAN_POINT('Ctrl Pts',(172.092351809097,-3.0579808723308,331.145556768763));
#48614=CARTESIAN_POINT('Ctrl Pts',(172.084593997575,-3.16296908120222,331.233727352692));
#48615=CARTESIAN_POINT('Ctrl Pts',(172.076842024052,-3.26787828311715,331.321831585461));
#48616=CARTESIAN_POINT('Ctrl Pts',(172.069090050529,-3.3691850820428,331.414391017976));
#48617=CARTESIAN_POINT('Ctrl Pts',(172.061338077006,-3.46649436303045,331.511074679278));
#48618=CARTESIAN_POINT('Ctrl Pts',(172.053589386448,-3.56376243347976,331.607717394991));
#48619=CARTESIAN_POINT('Ctrl Pts',(172.045840695891,-3.65703607644908,331.708480590676));
#48620=CARTESIAN_POINT('Ctrl Pts',(172.038092005333,-3.7459552276218,331.812994745038));
#48621=CARTESIAN_POINT('Ctrl Pts',(172.030344926955,-3.83485587842246,331.917487154358));
#48622=CARTESIAN_POINT('Ctrl Pts',(172.022597848577,-3.91940358637563,332.025728672528));
#48623=CARTESIAN_POINT('Ctrl Pts',(172.0148507702,-3.99927724007334,332.137315137929));
#48624=CARTESIAN_POINT('Ctrl Pts',(172.007103626894,-4.07915156318909,332.248902538532));
#48625=CARTESIAN_POINT('Ctrl Pts',(171.999356483588,-4.15435152640599,332.363834624441));
#48626=CARTESIAN_POINT('Ctrl Pts',(171.991609340282,-4.22459842473841,332.481676904725));
#48627=CARTESIAN_POINT('Ctrl Pts',(171.983860455254,-4.29486111606491,332.599545678454));
#48628=CARTESIAN_POINT('Ctrl Pts',(171.976111570226,-4.36016832655585,332.720325612808));
#48629=CARTESIAN_POINT('Ctrl Pts',(171.968362685198,-4.4202867219027,332.843556548696));
#48630=CARTESIAN_POINT('Ctrl Pts',(171.960605575423,-4.4804689275356,332.966918283173));
#48631=CARTESIAN_POINT('Ctrl Pts',(171.952848465648,-4.53545114469992,333.092735864107));
#48632=CARTESIAN_POINT('Ctrl Pts',(171.945091355874,-4.58504751919254,333.220527519391));
#48633=CARTESIAN_POINT('Ctrl Pts',(171.937330100948,-4.63467039640191,333.348387462449));
#48634=CARTESIAN_POINT('Ctrl Pts',(171.929568846021,-4.67890157023945,333.478223211998));
#48635=CARTESIAN_POINT('Ctrl Pts',(171.921807591095,-4.71760505331683,333.609537622437));
#48636=CARTESIAN_POINT('Ctrl Pts',(171.914033920691,-4.75637044935367,333.741062093136));
#48637=CARTESIAN_POINT('Ctrl Pts',(171.906260250286,-4.78959038992416,333.874069572022));
#48638=CARTESIAN_POINT('Ctrl Pts',(171.898486579881,-4.81717982817702,334.008051631634));
#48639=CARTESIAN_POINT('Ctrl Pts',(171.891074775704,-4.84348497144162,334.135796794137));
#48640=CARTESIAN_POINT('Ctrl Pts',(171.883662971527,-4.86467196859223,334.264427561831));
#48641=CARTESIAN_POINT('Ctrl Pts',(171.87625116735,-4.8807111744566,334.39350062322));
#48642=CARTESIAN_POINT('Ctrl Pts',(171.86477323707,-4.90554951101645,334.593383346012));
#48643=CARTESIAN_POINT('Ctrl Pts',(171.853295306789,-4.91811256346442,334.794822525422));
#48644=CARTESIAN_POINT('Ctrl Pts',(171.841817376508,-4.9182488785387,334.996678667015));
#48645=CARTESIAN_POINT('',(170.091817376553,-4.91824948312363,334.997745170935));
#48646=CARTESIAN_POINT('Ctrl Pts',(171.841817376472,-4.91824887853913,334.996678667656));
#48647=CARTESIAN_POINT('Ctrl Pts',(171.83415687076,-4.91833985680596,335.131399831482));
#48648=CARTESIAN_POINT('Ctrl Pts',(171.826496365047,-4.91289122752626,335.266338137322));
#48649=CARTESIAN_POINT('Ctrl Pts',(171.818835859335,-4.90187596891744,335.400992578298));
#48650=CARTESIAN_POINT('Ctrl Pts',(171.811183512138,-4.89087244166797,335.535503610962));
#48651=CARTESIAN_POINT('Ctrl Pts',(171.80353116494,-4.87431410850533,335.669730981874));
#48652=CARTESIAN_POINT('Ctrl Pts',(171.795878817742,-4.85222596571158,335.803172609203));
#48653=CARTESIAN_POINT('Ctrl Pts',(171.788232669823,-4.83015571684494,335.936506133521));
#48654=CARTESIAN_POINT('Ctrl Pts',(171.780586521903,-4.80256463531711,336.069054785126));
#48655=CARTESIAN_POINT('Ctrl Pts',(171.772940373984,-4.76952958216479,336.200321051784));
#48656=CARTESIAN_POINT('Ctrl Pts',(171.765297904939,-4.73651042352852,336.331524160868));
#48657=CARTESIAN_POINT('Ctrl Pts',(171.757655435894,-4.69805259911997,336.461445722151));
#48658=CARTESIAN_POINT('Ctrl Pts',(171.75001296685,-4.65428408820265,336.589598279064));
#48659=CARTESIAN_POINT('Ctrl Pts',(171.742372266164,-4.61052570469982,336.717721183288));
#48660=CARTESIAN_POINT('Ctrl Pts',(171.734731565479,-4.5614592076922,336.844075516026));
#48661=CARTESIAN_POINT('Ctrl Pts',(171.727090864793,-4.50726232661123,336.968189366299));
#48662=CARTESIAN_POINT('Ctrl Pts',(171.719450170526,-4.45306549105969,337.092303112306));
#48663=CARTESIAN_POINT('Ctrl Pts',(171.71180947626,-4.39373844137937,337.214176010574));
#48664=CARTESIAN_POINT('Ctrl Pts',(171.704168781993,-4.32950667472082,337.333357027128));
#48665=CARTESIAN_POINT('Ctrl Pts',(171.696526332425,-4.26526015206392,337.452565423202));
#48666=CARTESIAN_POINT('Ctrl Pts',(171.688883882858,-4.19610686327876,337.56908035365));
#48667=CARTESIAN_POINT('Ctrl Pts',(171.68124143329,-4.12231750568051,337.682476737058));
#48668=CARTESIAN_POINT('Ctrl Pts',(171.673591077707,-4.04845181394261,337.795990427565));
#48669=CARTESIAN_POINT('Ctrl Pts',(171.665940722124,-3.96994069795861,337.906378792117));
#48670=CARTESIAN_POINT('Ctrl Pts',(171.658290366541,-3.88709748584564,338.013246786779));
#48671=CARTESIAN_POINT('Ctrl Pts',(171.650635692359,-3.80420750902946,338.120175108049));
#48672=CARTESIAN_POINT('Ctrl Pts',(171.642981018177,-3.71698082689311,338.223578796079));
#48673=CARTESIAN_POINT('Ctrl Pts',(171.635326343995,-3.62576916716357,338.323098104021));
#48674=CARTESIAN_POINT('Ctrl Pts',(171.627660272187,-3.53442169546484,338.42276559382));
#48675=CARTESIAN_POINT('Ctrl Pts',(171.619994200378,-3.43907768254678,338.518536870929));
#48676=CARTESIAN_POINT('Ctrl Pts',(171.612328128571,-3.34012393277351,338.610090743487));
#48677=CARTESIAN_POINT('Ctrl Pts',(171.607556463406,-3.27853121977259,338.667077481328));
#48678=CARTESIAN_POINT('Ctrl Pts',(171.602784798241,-3.21554063039557,338.722431078597));
#48679=CARTESIAN_POINT('Ctrl Pts',(171.598013133076,-3.15125113667784,338.776082538304));
#48680=CARTESIAN_POINT('Ctrl Pts',(171.590238054298,-3.04649611698931,338.863503660994));
#48681=CARTESIAN_POINT('Ctrl Pts',(171.582462975519,-2.93793498948684,338.946700496503));
#48682=CARTESIAN_POINT('Ctrl Pts',(171.574687896741,-2.82594309640998,339.02532342531));
#48683=CARTESIAN_POINT('Ctrl Pts',(171.566922385692,-2.71408901648724,339.103849603598));
#48684=CARTESIAN_POINT('Ctrl Pts',(171.559156874643,-2.59881288796413,339.17781285181));
#48685=CARTESIAN_POINT('Ctrl Pts',(171.551391363594,-2.480524311526,339.246902659872));
#48686=CARTESIAN_POINT('Ctrl Pts',(171.543633552072,-2.36235301855613,339.315923965189));
#48687=CARTESIAN_POINT('Ctrl Pts',(171.53587574055,-2.24117555701862,339.380081250501));
#48688=CARTESIAN_POINT('Ctrl Pts',(171.528117929027,-2.11743150328736,339.439106542018));
#48689=CARTESIAN_POINT('Ctrl Pts',(171.520365955504,-1.99378057088057,339.498087415131));
#48690=CARTESIAN_POINT('Ctrl Pts',(171.512613981981,-1.86756724209513,339.551943813942));
#48691=CARTESIAN_POINT('Ctrl Pts',(171.504862008458,-1.73925644244831,339.600453248312));
#48692=CARTESIAN_POINT('Ctrl Pts',(171.497113317901,-1.61099998250131,339.648942138908));
#48693=CARTESIAN_POINT('Ctrl Pts',(171.489364627343,-1.48064818327629,339.692088430941));
#48694=CARTESIAN_POINT('Ctrl Pts',(171.481615936785,-1.348686535168,339.729717506612));
#48695=CARTESIAN_POINT('Ctrl Pts',(171.473868858408,-1.21675234278274,339.767338753241));
#48696=CARTESIAN_POINT('Ctrl Pts',(171.46612178003,-1.08320934339336,339.799444959649));
#48697=CARTESIAN_POINT('Ctrl Pts',(171.458374701652,-0.948558416906424,
339.825911312096));
#48698=CARTESIAN_POINT('Ctrl Pts',(171.450627558346,-0.813906361915053,
339.852377886356));
#48699=CARTESIAN_POINT('Ctrl Pts',(171.44288041504,-0.678146744841247,339.873204436991));
#48700=CARTESIAN_POINT('Ctrl Pts',(171.435133271735,-0.541790480690989,
339.888317311461));
#48701=CARTESIAN_POINT('Ctrl Pts',(171.427384386706,-0.405403560757368,
339.903433583627));
#48702=CARTESIAN_POINT('Ctrl Pts',(171.419635501678,-0.268420115245306,
339.912833580455));
#48703=CARTESIAN_POINT('Ctrl Pts',(171.41188661665,-0.131355623864658,339.916495577399));
#48704=CARTESIAN_POINT('Ctrl Pts',(171.404129506875,0.0058543491829664,
339.920161461223));
#48705=CARTESIAN_POINT('Ctrl Pts',(171.396372397101,0.143145148586016,339.918077168616));
#48706=CARTESIAN_POINT('Ctrl Pts',(171.388615287326,0.280001294611361,339.910273142862));
#48707=CARTESIAN_POINT('Ctrl Pts',(171.3808540324,0.416930572185307,339.902464946887));
#48708=CARTESIAN_POINT('Ctrl Pts',(171.373092777474,0.553424344803314,339.888930966077));
#48709=CARTESIAN_POINT('Ctrl Pts',(171.365331522547,0.688973800366967,339.869753398778));
#48710=CARTESIAN_POINT('Ctrl Pts',(171.357557852143,0.824740090884081,339.85054515362));
#48711=CARTESIAN_POINT('Ctrl Pts',(171.349784181738,0.959558661130566,339.825675352503));
#48712=CARTESIAN_POINT('Ctrl Pts',(171.342010511333,1.09293153545217,339.795277230913));
#48713=CARTESIAN_POINT('Ctrl Pts',(171.334598707156,1.22009587038676,339.766294149197));
#48714=CARTESIAN_POINT('Ctrl Pts',(171.327186902979,1.34594579689556,339.732285926021));
#48715=CARTESIAN_POINT('Ctrl Pts',(171.319775098802,1.47006555683976,339.693409242874));
#48716=CARTESIAN_POINT('Ctrl Pts',(171.312000020024,1.60026879595247,339.652627097678));
#48717=CARTESIAN_POINT('Ctrl Pts',(171.304224941245,1.72897944518697,339.606358311038));
#48718=CARTESIAN_POINT('Ctrl Pts',(171.296449862467,1.85570038280514,339.554729317068));
#48719=CARTESIAN_POINT('Ctrl Pts',(171.288684351418,1.98226538224199,339.503163855861));
#48720=CARTESIAN_POINT('Ctrl Pts',(171.280918840369,2.1068451832861,339.446251457695));
#48721=CARTESIAN_POINT('Ctrl Pts',(171.27315332932,2.22895701295995,339.384168529707));
#48722=CARTESIAN_POINT('Ctrl Pts',(171.265395517797,2.35094776839938,339.322147157123));
#48723=CARTESIAN_POINT('Ctrl Pts',(171.257637706275,2.47047507595442,339.254965632935));
#48724=CARTESIAN_POINT('Ctrl Pts',(171.249879894753,2.58707571074669,339.182848590299));
#48725=CARTESIAN_POINT('Ctrl Pts',(171.24212792123,2.70358859986355,339.110785818024));
#48726=CARTESIAN_POINT('Ctrl Pts',(171.234375947707,2.81717886892489,339.033795124881));
#48727=CARTESIAN_POINT('Ctrl Pts',(171.226623974184,2.92740782335127,338.952147074475));
#48728=CARTESIAN_POINT('Ctrl Pts',(171.218875283626,3.03759009574995,338.870533602067));
#48729=CARTESIAN_POINT('Ctrl Pts',(171.211126593069,3.14441357135188,338.784266927518));
#48730=CARTESIAN_POINT('Ctrl Pts',(171.203377902511,3.24746868361462,338.693660814347));
#48731=CARTESIAN_POINT('Ctrl Pts',(171.195630824133,3.35050235440044,338.603073552535));
#48732=CARTESIAN_POINT('Ctrl Pts',(171.187883745755,3.44976892799036,338.508148905874));
#48733=CARTESIAN_POINT('Ctrl Pts',(171.180136667377,3.54489239098842,338.409240531088));
#48734=CARTESIAN_POINT('Ctrl Pts',(171.172389524072,3.64001665121254,338.310331327354));
#48735=CARTESIAN_POINT('Ctrl Pts',(171.164642380766,3.7309974606398,338.207438610628));
#48736=CARTESIAN_POINT('Ctrl Pts',(171.15689523746,3.81749639785324,338.100952162623));
#48737=CARTESIAN_POINT('Ctrl Pts',(171.149146352432,3.90401478186425,337.994441774204));
#48738=CARTESIAN_POINT('Ctrl Pts',(171.141397467404,3.98604904221244,337.884336350115));
#48739=CARTESIAN_POINT('Ctrl Pts',(171.133648582376,4.06330195461183,337.771057611842));
#48740=CARTESIAN_POINT('Ctrl Pts',(171.125891472601,4.14063686405067,337.657658638346));
#48741=CARTESIAN_POINT('Ctrl Pts',(171.118134362826,4.21318006723221,337.54107994583));
#48742=CARTESIAN_POINT('Ctrl Pts',(171.110377253052,4.28067820890297,337.421771486809));
#48743=CARTESIAN_POINT('Ctrl Pts',(171.102615998125,4.34821241942249,337.302399273163));
#48744=CARTESIAN_POINT('Ctrl Pts',(171.094854743199,4.41069601859924,337.180294734205));
#48745=CARTESIAN_POINT('Ctrl Pts',(171.087093488273,4.46792278135317,337.055930223127));
#48746=CARTESIAN_POINT('Ctrl Pts',(171.079319817868,4.52524108827738,336.93136676936));
#48747=CARTESIAN_POINT('Ctrl Pts',(171.071546147464,4.57728560619161,336.804536480998));
#48748=CARTESIAN_POINT('Ctrl Pts',(171.063772477059,4.62389889246094,336.675930217759));
#48749=CARTESIAN_POINT('Ctrl Pts',(171.056360672882,4.66834231903945,336.553310607017));
#48750=CARTESIAN_POINT('Ctrl Pts',(171.048948868705,4.70784869513809,336.429076917974));
#48751=CARTESIAN_POINT('Ctrl Pts',(171.041537064528,4.74232478697736,336.303663559865));
#48752=CARTESIAN_POINT('Ctrl Pts',(171.03376198575,4.77849065477695,336.172103319487));
#48753=CARTESIAN_POINT('Ctrl Pts',(171.025986906971,4.80923496270685,336.038829093271));
#48754=CARTESIAN_POINT('Ctrl Pts',(171.018211828193,4.83439501081193,335.904327342248));
#48755=CARTESIAN_POINT('Ctrl Pts',(171.010446317144,4.85952409787605,335.769991104191));
#48756=CARTESIAN_POINT('Ctrl Pts',(171.002680806095,4.87908252681788,335.63443072742));
#48757=CARTESIAN_POINT('Ctrl Pts',(170.994915295046,4.89295738600349,335.498147650054));
#48758=CARTESIAN_POINT('Ctrl Pts',(170.987157483524,4.90681848822583,335.361999697755));
#48759=CARTESIAN_POINT('Ctrl Pts',(170.979399672001,4.91500719587485,335.225130857216));
#48760=CARTESIAN_POINT('Ctrl Pts',(170.971641860479,4.91746173020135,335.088052226009));
#48761=CARTESIAN_POINT('Ctrl Pts',(170.963889886956,4.91991441741294,334.951076750818));
#48762=CARTESIAN_POINT('Ctrl Pts',(170.956137913433,4.916641513422,334.813892188438));
#48763=CARTESIAN_POINT('Ctrl Pts',(170.94838593991,4.9076331381274,334.677013863991));
#48764=CARTESIAN_POINT('Ctrl Pts',(170.940637249353,4.89862857788507,334.540193507596));
#48765=CARTESIAN_POINT('Ctrl Pts',(170.932888558795,4.88389340301586,334.403679520404));
#48766=CARTESIAN_POINT('Ctrl Pts',(170.925139868237,4.86346982400044,334.267986111104));
#48767=CARTESIAN_POINT('Ctrl Pts',(170.917392789859,4.84305049428122,334.13232093395));
#48768=CARTESIAN_POINT('Ctrl Pts',(170.909645711482,4.81694517266051,333.997476381376));
#48769=CARTESIAN_POINT('Ctrl Pts',(170.901898633104,4.78524777419646,333.863960035013));
#48770=CARTESIAN_POINT('Ctrl Pts',(170.894151489798,4.75355011007767,333.730442569654));
#48771=CARTESIAN_POINT('Ctrl Pts',(170.886404346492,4.71626036592176,333.598253713012));
#48772=CARTESIAN_POINT('Ctrl Pts',(170.878657203186,4.67352317824004,333.467888984129));
#48773=CARTESIAN_POINT('Ctrl Pts',(170.870908318158,4.63077638233125,333.337494946487));
#48774=CARTESIAN_POINT('Ctrl Pts',(170.86315943313,4.58257982761819,333.208926224014));
#48775=CARTESIAN_POINT('Ctrl Pts',(170.855410548102,4.52912730357899,333.082660976646));
#48776=CARTESIAN_POINT('Ctrl Pts',(170.847653438327,4.47561804447848,332.956261710041));
#48777=CARTESIAN_POINT('Ctrl Pts',(170.839896328553,4.4168418246148,332.83217116304));
#48778=CARTESIAN_POINT('Ctrl Pts',(170.832139218778,4.35303991359075,332.710845882605));
#48779=CARTESIAN_POINT('Ctrl Pts',(170.824377963852,4.2892039088655,332.58945576982));
#48780=CARTESIAN_POINT('Ctrl Pts',(170.816616708926,4.22033705789302,332.470834205856));
#48781=CARTESIAN_POINT('Ctrl Pts',(170.808855453999,4.14672497232374,332.355410227198));
#48782=CARTESIAN_POINT('Ctrl Pts',(170.801081783595,4.07299513140762,332.239801607791));
#48783=CARTESIAN_POINT('Ctrl Pts',(170.79330811319,3.99450511107566,332.127401115803));
#48784=CARTESIAN_POINT('Ctrl Pts',(170.785534442786,3.91158248449447,332.018606780464));
#48785=CARTESIAN_POINT('Ctrl Pts',(170.778122638608,3.83251992612982,331.914876847608));
#48786=CARTESIAN_POINT('Ctrl Pts',(170.770710834431,3.74942833358566,331.814425115445));
#48787=CARTESIAN_POINT('Ctrl Pts',(170.763299030254,3.66262255670514,331.717565070011));
#48788=CARTESIAN_POINT('Ctrl Pts',(170.755523951476,3.57156217011946,331.615957625219));
#48789=CARTESIAN_POINT('Ctrl Pts',(170.747748872697,3.4761265391429,331.517981749701));
#48790=CARTESIAN_POINT('Ctrl Pts',(170.739973793919,3.3766366929507,331.424037513295));
#48791=CARTESIAN_POINT('Ctrl Pts',(170.73220828287,3.27726927534811,331.330208881253));
#48792=CARTESIAN_POINT('Ctrl Pts',(170.724442771821,3.17385785062971,331.240402282771));
#48793=CARTESIAN_POINT('Ctrl Pts',(170.716677260772,3.06676298584503,331.154984024591));
#48794=CARTESIAN_POINT('Ctrl Pts',(170.708919449249,2.95977430593056,331.069650458862));
#48795=CARTESIAN_POINT('Ctrl Pts',(170.701161637727,2.84910975752933,330.988696816753));
#48796=CARTESIAN_POINT('Ctrl Pts',(170.693403826205,2.73516570146764,330.912451633556));
#48797=CARTESIAN_POINT('Ctrl Pts',(170.685651852682,2.62130739192161,330.836263827278));
#48798=CARTESIAN_POINT('Ctrl Pts',(170.677899879159,2.504174810563,330.764777643716));
#48799=CARTESIAN_POINT('Ctrl Pts',(170.670147905636,2.38419595859192,330.698280263251));
#48800=CARTESIAN_POINT('Ctrl Pts',(170.662399215078,2.26426791773581,330.631811044467));
#48801=CARTESIAN_POINT('Ctrl Pts',(170.654650524521,2.14149634488201,330.570326615735));
#48802=CARTESIAN_POINT('Ctrl Pts',(170.646901833963,2.01633649159924,330.514069749189));
#48803=CARTESIAN_POINT('Ctrl Pts',(170.639154755585,1.89120267886925,330.457824587353));
#48804=CARTESIAN_POINT('Ctrl Pts',(170.631407677207,1.76368193037506,330.40680498446));
#48805=CARTESIAN_POINT('Ctrl Pts',(170.62366059883,1.63425190516625,330.361206646879));
#48806=CARTESIAN_POINT('Ctrl Pts',(170.615913455524,1.5048207952092,330.31560792714));
#48807=CARTESIAN_POINT('Ctrl Pts',(170.608166312218,1.37348074528588,330.275430693219));
#48808=CARTESIAN_POINT('Ctrl Pts',(170.600419168912,1.24072671904426,330.240821470973));
#48809=CARTESIAN_POINT('Ctrl Pts',(170.592670283884,1.10794284687953,330.20620446784));
#48810=CARTESIAN_POINT('Ctrl Pts',(170.584921398856,0.973744743985446,330.177158065924));
#48811=CARTESIAN_POINT('Ctrl Pts',(170.577172513828,0.838639375860506,330.1537780633));
#48812=CARTESIAN_POINT('Ctrl Pts',(170.569415404053,0.703390605501616,330.130373244899));
#48813=CARTESIAN_POINT('Ctrl Pts',(170.561658294278,0.567233032025835,330.112646906821));
#48814=CARTESIAN_POINT('Ctrl Pts',(170.553901184504,0.430681140338857,330.100643224069));
#48815=CARTESIAN_POINT('Ctrl Pts',(170.546139929578,0.294056279686859,330.088633126933));
#48816=CARTESIAN_POINT('Ctrl Pts',(170.538378674651,0.157037071229068,330.082351796361));
#48817=CARTESIAN_POINT('Ctrl Pts',(170.530617419725,0.0201388617503955,
330.081791231683));
#48818=CARTESIAN_POINT('Ctrl Pts',(170.52284374932,-0.116978340248281,330.081229770284));
#48819=CARTESIAN_POINT('Ctrl Pts',(170.515070078916,-0.253973765678893,
330.086407347139));
#48820=CARTESIAN_POINT('Ctrl Pts',(170.507296408511,-0.390335434633327,
330.097263895439));
#48821=CARTESIAN_POINT('Ctrl Pts',(170.499884604334,-0.520349435090383,
330.107615068803));
#48822=CARTESIAN_POINT('Ctrl Pts',(170.492472800157,-0.649787068228315,
330.123128365462));
#48823=CARTESIAN_POINT('Ctrl Pts',(170.48506099598,-0.778214333635241,330.143708666747));
#48824=CARTESIAN_POINT('Ctrl Pts',(170.477285917202,-0.912936201885633,
330.165297669905));
#48825=CARTESIAN_POINT('Ctrl Pts',(170.469510838423,-1.04697190184907,330.192531159925));
#48826=CARTESIAN_POINT('Ctrl Pts',(170.461735759645,-1.17981127895567,330.225355677273));
#48827=CARTESIAN_POINT('Ctrl Pts',(170.453970248596,-1.31248718875235,330.258139801962));
#48828=CARTESIAN_POINT('Ctrl Pts',(170.446204737547,-1.44396932901759,330.296501171654));
#48829=CARTESIAN_POINT('Ctrl Pts',(170.438439226498,-1.5737545410778,330.340334807421));
#48830=CARTESIAN_POINT('Ctrl Pts',(170.430681414975,-1.70341107072154,330.384124982009));
#48831=CARTESIAN_POINT('Ctrl Pts',(170.422923603453,-1.8313736525109,330.43337650082));
#48832=CARTESIAN_POINT('Ctrl Pts',(170.415165791931,-1.95715152052411,330.487933844877));
#48833=CARTESIAN_POINT('Ctrl Pts',(170.407413818408,-2.08283473670317,330.542450132802));
#48834=CARTESIAN_POINT('Ctrl Pts',(170.399661844885,-2.20633615439062,330.602264143578));
#48835=CARTESIAN_POINT('Ctrl Pts',(170.391909871362,-2.32718266146913,330.667171371649));
#48836=CARTESIAN_POINT('Ctrl Pts',(170.384161180805,-2.44797798998007,330.73205111147));
#48837=CARTESIAN_POINT('Ctrl Pts',(170.376412490247,-2.56612030051568,330.802019593937));
#48838=CARTESIAN_POINT('Ctrl Pts',(170.368663799689,-2.68115907806432,330.876825366224));
#48839=CARTESIAN_POINT('Ctrl Pts',(170.360916721311,-2.79617392083476,330.951615574546));
#48840=CARTESIAN_POINT('Ctrl Pts',(170.353169642934,-2.9080861875124,331.031240857861));
#48841=CARTESIAN_POINT('Ctrl Pts',(170.345422564556,-3.01647281571578,331.11540545043));
#48842=CARTESIAN_POINT('Ctrl Pts',(170.33767542125,-3.12486035230351,331.19957074838));
#48843=CARTESIAN_POINT('Ctrl Pts',(170.329928277944,-3.2297218827555,331.288275191734));
#48844=CARTESIAN_POINT('Ctrl Pts',(170.322181134638,-3.33066633712121,331.381181848549));
#48845=CARTESIAN_POINT('Ctrl Pts',(170.31443224961,-3.43163348594351,331.474109392754));
#48846=CARTESIAN_POINT('Ctrl Pts',(170.306683364582,-3.52868151875388,331.571240765711));
#48847=CARTESIAN_POINT('Ctrl Pts',(170.298934479554,-3.62145552878866,331.67220149115));
#48848=CARTESIAN_POINT('Ctrl Pts',(170.291177369779,-3.71432801011585,331.773269377345));
#48849=CARTESIAN_POINT('Ctrl Pts',(170.283420260005,-3.8029171417072,331.878174447005));
#48850=CARTESIAN_POINT('Ctrl Pts',(170.27566315023,-3.88690735855828,331.986507964423));
#48851=CARTESIAN_POINT('Ctrl Pts',(170.267901895304,-3.97094245709576,332.094899371809));
#48852=CARTESIAN_POINT('Ctrl Pts',(170.260140640377,-4.05037351783678,332.206722558982));
#48853=CARTESIAN_POINT('Ctrl Pts',(170.252379385451,-4.12492838499993,332.321539830215));
#48854=CARTESIAN_POINT('Ctrl Pts',(170.244605715047,-4.19960251565316,332.436540771664));
#48855=CARTESIAN_POINT('Ctrl Pts',(170.236832044642,-4.26938466631352,332.554545031503));
#48856=CARTESIAN_POINT('Ctrl Pts',(170.229058374237,-4.33404828673625,332.675089569308));
#48857=CARTESIAN_POINT('Ctrl Pts',(170.22164657006,-4.39570180007076,332.790022729877));
#48858=CARTESIAN_POINT('Ctrl Pts',(170.214234765883,-4.45270246836924,332.907264731988));
#48859=CARTESIAN_POINT('Ctrl Pts',(170.206822961706,-4.50489541642322,333.026399141268));
#48860=CARTESIAN_POINT('Ctrl Pts',(170.198248995252,-4.5652721580458,333.164213687401));
#48861=CARTESIAN_POINT('Ctrl Pts',(170.189675028798,-4.61937956341198,333.304934489102));
#48862=CARTESIAN_POINT('Ctrl Pts',(170.181101062344,-4.66695640459487,333.448000972903));
#48863=CARTESIAN_POINT('Ctrl Pts',(170.172560704663,-4.71434675107962,333.590506655691));
#48864=CARTESIAN_POINT('Ctrl Pts',(170.164020346983,-4.75525750505167,333.735339441107));
#48865=CARTESIAN_POINT('Ctrl Pts',(170.155479989303,-4.78947631491731,333.881921428814));
#48866=CARTESIAN_POINT('Ctrl Pts',(170.146961338724,-4.82360815053345,334.028130847795));
#48867=CARTESIAN_POINT('Ctrl Pts',(170.138442688146,-4.85108189296937,334.176080358734));
#48868=CARTESIAN_POINT('Ctrl Pts',(170.129924037567,-4.87173436043102,334.325176034883));
#48869=CARTESIAN_POINT('Ctrl Pts',(170.12143967778,-4.89230369389797,334.47367154453));
#48870=CARTESIAN_POINT('Ctrl Pts',(170.112955317993,-4.90610646026499,334.623303768268));
#48871=CARTESIAN_POINT('Ctrl Pts',(170.104470958206,-4.91303031194559,334.773469171184));
#48872=CARTESIAN_POINT('Ctrl Pts',(170.100253097655,-4.91647239144224,334.84812144254));
#48873=CARTESIAN_POINT('Ctrl Pts',(170.096035237104,-4.9182151718842,334.92290524704));
#48874=CARTESIAN_POINT('Ctrl Pts',(170.091817376553,-4.91824948312363,334.997745170935));
#48875=CARTESIAN_POINT('',(168.341817376469,-4.91824814939194,335.004266556313));
#48876=CARTESIAN_POINT('Ctrl Pts',(170.091817376508,-4.918249483124,334.997745171737));
#48877=CARTESIAN_POINT('Ctrl Pts',(170.083938194233,-4.91831357827607,335.137550031252));
#48878=CARTESIAN_POINT('Ctrl Pts',(170.076059011959,-4.91241223784542,335.277335856181));
#48879=CARTESIAN_POINT('Ctrl Pts',(170.068179829684,-4.90057678679853,335.416569585053));
#48880=CARTESIAN_POINT('Ctrl Pts',(170.060297759064,-4.88873699711906,335.555854354142));
#48881=CARTESIAN_POINT('Ctrl Pts',(170.052415688443,-4.87095879426482,335.694586253213));
#48882=CARTESIAN_POINT('Ctrl Pts',(170.044533617822,-4.84732532250688,335.832238115135));
#48883=CARTESIAN_POINT('Ctrl Pts',(170.036647192215,-4.82367879282824,335.969966032201));
#48884=CARTESIAN_POINT('Ctrl Pts',(170.028760766608,-4.79417061176356,336.106612356849));
#48885=CARTESIAN_POINT('Ctrl Pts',(170.020874341001,-4.75893485644403,336.24166102243));
#48886=CARTESIAN_POINT('Ctrl Pts',(170.012976316539,-4.72364727861164,336.376908309018));
#48887=CARTESIAN_POINT('Ctrl Pts',(170.005078292078,-4.68261539016203,336.510552881302));
#48888=CARTESIAN_POINT('Ctrl Pts',(169.997180267616,-4.63602320102892,336.642093767731));
#48889=CARTESIAN_POINT('Ctrl Pts',(169.989276218659,-4.58939547206374,336.773734991601));
#48890=CARTESIAN_POINT('Ctrl Pts',(169.981372169701,-4.53719912558592,336.903268985875));
#48891=CARTESIAN_POINT('Ctrl Pts',(169.973468120743,-4.47966576469273,337.030216170544));
#48892=CARTESIAN_POINT('Ctrl Pts',(169.96554943329,-4.42202585058367,337.157398464558));
#48893=CARTESIAN_POINT('Ctrl Pts',(169.957630745837,-4.35902933402799,337.281984041251));
#48894=CARTESIAN_POINT('Ctrl Pts',(169.949712058384,-4.29095368250246,337.403518162427));
#48895=CARTESIAN_POINT('Ctrl Pts',(169.9426696814,-4.23041152771796,337.511602880105));
#48896=CARTESIAN_POINT('Ctrl Pts',(169.935627304416,-4.16585291978915,337.617274393364));
#48897=CARTESIAN_POINT('Ctrl Pts',(169.928584927432,-4.09750046770699,337.720233993546));
#48898=CARTESIAN_POINT('Ctrl Pts',(169.920809848654,-4.02203650137134,337.833905699027));
#48899=CARTESIAN_POINT('Ctrl Pts',(169.913034769875,-3.94171953061327,337.944614398106));
#48900=CARTESIAN_POINT('Ctrl Pts',(169.905259691097,-3.85680956688121,338.051917926045));
#48901=CARTESIAN_POINT('Ctrl Pts',(169.897494180048,-3.77200409026515,338.159089410162));
#48902=CARTESIAN_POINT('Ctrl Pts',(169.889728668999,-3.68261710670557,338.262863757008));
#48903=CARTESIAN_POINT('Ctrl Pts',(169.88196315795,-3.58895261920911,338.362826513451));
#48904=CARTESIAN_POINT('Ctrl Pts',(169.874205346428,-3.49538100032463,338.462690156531));
#48905=CARTESIAN_POINT('Ctrl Pts',(169.866447534905,-3.39754058318325,338.558749446645));
#48906=CARTESIAN_POINT('Ctrl Pts',(169.858689723383,-3.29577623510711,338.650622148429));
#48907=CARTESIAN_POINT('Ctrl Pts',(169.85093774986,-3.19408846793019,338.742425713092));
#48908=CARTESIAN_POINT('Ctrl Pts',(169.843185776337,-3.08848293634901,338.830048699548));
#48909=CARTESIAN_POINT('Ctrl Pts',(169.835433802814,-2.97934177848387,338.913145234908));
#48910=CARTESIAN_POINT('Ctrl Pts',(169.827685112256,-2.87024684196379,338.996206578835));
#48911=CARTESIAN_POINT('Ctrl Pts',(169.819936421699,-2.75761956761028,339.074745048066));
#48912=CARTESIAN_POINT('Ctrl Pts',(169.812187731141,-2.64187546028209,339.148454786407));
#48913=CARTESIAN_POINT('Ctrl Pts',(169.804440652763,-2.5261554344821,339.22214918882));
#48914=CARTESIAN_POINT('Ctrl Pts',(169.796693574386,-2.40732019507464,339.291016648849));
#48915=CARTESIAN_POINT('Ctrl Pts',(169.788946496008,-2.28581420439046,339.354794654804));
#48916=CARTESIAN_POINT('Ctrl Pts',(169.781199352702,-2.16430719536891,339.418573195279));
#48917=CARTESIAN_POINT('Ctrl Pts',(169.773452209396,-2.04012973651922,339.477262014939));
#48918=CARTESIAN_POINT('Ctrl Pts',(169.76570506609,-1.91375050286465,339.530644774785));
#48919=CARTESIAN_POINT('Ctrl Pts',(169.757956181062,-1.78734285647576,339.584039536208));
#48920=CARTESIAN_POINT('Ctrl Pts',(169.750207296034,-1.65873281027521,339.632125711985));
#48921=CARTESIAN_POINT('Ctrl Pts',(169.742458411006,-1.52840822762592,339.674735431254));
#48922=CARTESIAN_POINT('Ctrl Pts',(169.734701301231,-1.39794531711777,339.71739037692));
#48923=CARTESIAN_POINT('Ctrl Pts',(169.726944191456,-1.26576460699429,339.754557132868));
#48924=CARTESIAN_POINT('Ctrl Pts',(169.719187081682,-1.13236884236745,339.786117828401));
#48925=CARTESIAN_POINT('Ctrl Pts',(169.711425826756,-0.99890179530943,339.81769538896));
#48926=CARTESIAN_POINT('Ctrl Pts',(169.703664571829,-0.864218783598727,
339.843660845948));
#48927=CARTESIAN_POINT('Ctrl Pts',(169.695903316903,-0.728830925740224,
339.863947835266));
#48928=CARTESIAN_POINT('Ctrl Pts',(169.688129646499,-0.593226491431694,
339.884267277155));
#48929=CARTESIAN_POINT('Ctrl Pts',(169.680355976094,-0.456915346697097,
339.898890057743));
#48930=CARTESIAN_POINT('Ctrl Pts',(169.672582305689,-0.320412783048802,
339.907801820669));
#48931=CARTESIAN_POINT('Ctrl Pts',(169.665170501512,-0.190264446579206,
339.916298738886));
#48932=CARTESIAN_POINT('Ctrl Pts',(169.657758697335,-0.0599423989477547,
339.919604362407));
#48933=CARTESIAN_POINT('Ctrl Pts',(169.650346893158,0.0701101812161591,
339.917750260535));
#48934=CARTESIAN_POINT('Ctrl Pts',(169.64257181438,0.206537025740678,339.915805283607));
#48935=CARTESIAN_POINT('Ctrl Pts',(169.634796735601,0.343098454126135,339.908175858945));
#48936=CARTESIAN_POINT('Ctrl Pts',(169.627021656823,0.479281933498523,339.894841355011));
#48937=CARTESIAN_POINT('Ctrl Pts',(169.619256145774,0.615297830429725,339.881523260033));
#48938=CARTESIAN_POINT('Ctrl Pts',(169.611490634725,0.750936318449167,339.862514092219));
#48939=CARTESIAN_POINT('Ctrl Pts',(169.603725123676,0.885684361606167,339.837845209813));
#48940=CARTESIAN_POINT('Ctrl Pts',(169.595967312154,1.02029880168614,339.813200786675));
#48941=CARTESIAN_POINT('Ctrl Pts',(169.588209500632,1.15402417187472,339.782907886328));
#48942=CARTESIAN_POINT('Ctrl Pts',(169.580451689109,1.28635241480442,339.747049665574));
#48943=CARTESIAN_POINT('Ctrl Pts',(169.572699715586,1.41858107653441,339.711218429268));
#48944=CARTESIAN_POINT('Ctrl Pts',(169.564947742063,1.54941432798192,339.669830310544));
#48945=CARTESIAN_POINT('Ctrl Pts',(169.557195768541,1.67835452039141,339.623019485832));
#48946=CARTESIAN_POINT('Ctrl Pts',(169.549447077983,1.80724010655317,339.576228485532));
#48947=CARTESIAN_POINT('Ctrl Pts',(169.541698387425,1.93423386157843,339.524019479968));
#48948=CARTESIAN_POINT('Ctrl Pts',(169.533949696868,2.05885373094771,339.466576359704));
#48949=CARTESIAN_POINT('Ctrl Pts',(169.52620261849,2.18344767211244,339.40914519096));
#48950=CARTESIAN_POINT('Ctrl Pts',(169.518455540112,2.30566835528164,339.346482237139));
#48951=CARTESIAN_POINT('Ctrl Pts',(169.510708461734,2.42505450470427,339.27881919596));
#48952=CARTESIAN_POINT('Ctrl Pts',(169.502961318429,2.54444165469767,339.211155587699));
#48953=CARTESIAN_POINT('Ctrl Pts',(169.495214175123,2.66099388350513,339.138492001224));
#48954=CARTESIAN_POINT('Ctrl Pts',(169.487467031817,2.77427564009967,339.061105481916));
#48955=CARTESIAN_POINT('Ctrl Pts',(169.479718146789,2.8875828648381,338.983701564476));
#48956=CARTESIAN_POINT('Ctrl Pts',(169.471969261761,2.997617831565,338.901572821748));
#48957=CARTESIAN_POINT('Ctrl Pts',(169.464220376733,3.10397536323157,338.815038663887));
#48958=CARTESIAN_POINT('Ctrl Pts',(169.456463266958,3.2104457838812,338.728412657776));
#48959=CARTESIAN_POINT('Ctrl Pts',(169.448706157183,3.31323066865106,338.637372142953));
#48960=CARTESIAN_POINT('Ctrl Pts',(169.440949047409,3.41195883332961,338.54227610191));
#48961=CARTESIAN_POINT('Ctrl Pts',(169.433187792482,3.51073975518256,338.447129244583));
#48962=CARTESIAN_POINT('Ctrl Pts',(169.425426537556,3.60545936765833,338.347922825373));
#48963=CARTESIAN_POINT('Ctrl Pts',(169.41766528263,3.6957852682207,338.245050741314));
#48964=CARTESIAN_POINT('Ctrl Pts',(169.409891612225,3.78625566078692,338.142014095446));
#48965=CARTESIAN_POINT('Ctrl Pts',(169.402117941821,3.87231805089456,338.035300371399));
#48966=CARTESIAN_POINT('Ctrl Pts',(169.394344271416,3.95368151216845,337.925335119749));
#48967=CARTESIAN_POINT('Ctrl Pts',(169.386932467239,4.03125748474596,337.820488777018));
#48968=CARTESIAN_POINT('Ctrl Pts',(169.379520663062,4.10456199193852,337.712687049428));
#48969=CARTESIAN_POINT('Ctrl Pts',(169.372108858885,4.17338175166202,337.602319699306));
#48970=CARTESIAN_POINT('Ctrl Pts',(169.364333780106,4.24557457281241,337.486542916587));
#48971=CARTESIAN_POINT('Ctrl Pts',(169.356558701328,4.3130600516395,337.367576778586));
#48972=CARTESIAN_POINT('Ctrl Pts',(169.348783622549,4.37554347769722,337.245841120222));
#48973=CARTESIAN_POINT('Ctrl Pts',(169.3410181115,4.43795001392124,337.124255265336));
#48974=CARTESIAN_POINT('Ctrl Pts',(169.333252600451,4.49536656796597,336.99990701559));
#48975=CARTESIAN_POINT('Ctrl Pts',(169.325487089402,4.54754187645625,336.873244763606));
#48976=CARTESIAN_POINT('Ctrl Pts',(169.31772927788,4.59966545297627,336.746708097613));
#48977=CARTESIAN_POINT('Ctrl Pts',(169.309971466358,4.64655797777329,336.617862354332));
#48978=CARTESIAN_POINT('Ctrl Pts',(169.302213654836,4.68801444018168,336.487179770958));
#48979=CARTESIAN_POINT('Ctrl Pts',(169.294461681313,4.72943970528746,336.356595530373));
#48980=CARTESIAN_POINT('Ctrl Pts',(169.28670970779,4.76543693284398,336.224177572134));
#48981=CARTESIAN_POINT('Ctrl Pts',(169.278957734266,4.79584964837816,336.090416990262));
#48982=CARTESIAN_POINT('Ctrl Pts',(169.271209043709,4.82624948410928,335.956713056075));
#48983=CARTESIAN_POINT('Ctrl Pts',(169.263460353151,4.85106942524451,335.821668009518));
#48984=CARTESIAN_POINT('Ctrl Pts',(169.255711662594,4.87020324192108,335.685786734256));
#48985=CARTESIAN_POINT('Ctrl Pts',(169.247964584216,4.88933307764727,335.549933730228));
#48986=CARTESIAN_POINT('Ctrl Pts',(169.240217505838,4.90277908760817,335.413245230375));
#48987=CARTESIAN_POINT('Ctrl Pts',(169.23247042746,4.91048648858074,335.276234516247));
#48988=CARTESIAN_POINT('Ctrl Pts',(169.224723284154,4.91819395414874,335.139222653837));
#48989=CARTESIAN_POINT('Ctrl Pts',(169.216976140848,4.92016269284566,335.001888962022));
#48990=CARTESIAN_POINT('Ctrl Pts',(169.209228997542,4.91638997638955,334.864749630106));
#48991=CARTESIAN_POINT('Ctrl Pts',(169.201480112514,4.91261641174668,334.727579466357));
#48992=CARTESIAN_POINT('Ctrl Pts',(169.193731227486,4.90309883414778,334.590604140107));
#48993=CARTESIAN_POINT('Ctrl Pts',(169.185982342458,4.88788657785546,334.454337224542));
#48994=CARTESIAN_POINT('Ctrl Pts',(169.178225232683,4.87265817511715,334.317925673865));
#48995=CARTESIAN_POINT('Ctrl Pts',(169.170468122909,4.85172306288239,334.182224424969));
#48996=CARTESIAN_POINT('Ctrl Pts',(169.162711013134,4.82518224811235,334.047739880599));
#48997=CARTESIAN_POINT('Ctrl Pts',(169.154949758208,4.79862725077952,333.913183471989));
#48998=CARTESIAN_POINT('Ctrl Pts',(169.147188503281,4.76646067371024,333.779845443206));
#48999=CARTESIAN_POINT('Ctrl Pts',(169.139427248355,4.72883387123818,333.648218478921));
#49000=CARTESIAN_POINT('Ctrl Pts',(169.131653577951,4.69114687814468,333.51638095439));
#49001=CARTESIAN_POINT('Ctrl Pts',(169.123879907546,4.64798232850219,333.386260335174));
#49002=CARTESIAN_POINT('Ctrl Pts',(169.116106237141,4.59954063991313,333.258331557303));
#49003=CARTESIAN_POINT('Ctrl Pts',(169.108694432964,4.55335392358308,333.136357894821));
#49004=CARTESIAN_POINT('Ctrl Pts',(169.101282628787,4.50237042605856,333.016376870382));
#49005=CARTESIAN_POINT('Ctrl Pts',(169.09387082461,4.44680248762131,332.8987787602));
#49006=CARTESIAN_POINT('Ctrl Pts',(169.086095745832,4.38851099899199,332.77541681633));
#49007=CARTESIAN_POINT('Ctrl Pts',(169.078320667054,4.324990100425,332.654287433897));
#49008=CARTESIAN_POINT('Ctrl Pts',(169.070545588275,4.25643335532864,332.535865637968));
#49009=CARTESIAN_POINT('Ctrl Pts',(169.062780077226,4.18796097367172,332.417589567599));
#49010=CARTESIAN_POINT('Ctrl Pts',(169.055014566177,4.11446526956193,332.302014789336));
#49011=CARTESIAN_POINT('Ctrl Pts',(169.047249055128,4.03618733289036,332.189595246888));
#49012=CARTESIAN_POINT('Ctrl Pts',(169.039491243606,3.95798700902063,332.077287168743));
#49013=CARTESIAN_POINT('Ctrl Pts',(169.031733432084,3.87501411055228,331.968128419376));
#49014=CARTESIAN_POINT('Ctrl Pts',(169.023975620561,3.78755480878344,331.862546951274));
#49015=CARTESIAN_POINT('Ctrl Pts',(169.016223647039,3.70016132291305,331.757044936575));
#49016=CARTESIAN_POINT('Ctrl Pts',(169.008471673515,3.60828840216793,331.655115144611));
#49017=CARTESIAN_POINT('Ctrl Pts',(169.000719699993,3.51226434067182,331.55715491726));
#49018=CARTESIAN_POINT('Ctrl Pts',(168.992971009435,3.4162809454227,331.459236176124));
#49019=CARTESIAN_POINT('Ctrl Pts',(168.985222318877,3.31615017902988,331.365283934538));
#49020=CARTESIAN_POINT('Ctrl Pts',(168.97747362832,3.21223912186442,331.275660744983));
#49021=CARTESIAN_POINT('Ctrl Pts',(168.969726549942,3.10834968426226,331.18605620228));
#49022=CARTESIAN_POINT('Ctrl Pts',(168.961979471564,3.00068181613677,331.100779175191));
#49023=CARTESIAN_POINT('Ctrl Pts',(168.954232393186,2.88963750054809,331.020153498195));
#49024=CARTESIAN_POINT('Ctrl Pts',(168.946485249881,2.77859225430122,330.939527145479));
#49025=CARTESIAN_POINT('Ctrl Pts',(168.938738106575,2.66417082044428,330.863552450261));
#49026=CARTESIAN_POINT('Ctrl Pts',(168.930990963269,2.54680579714443,330.792511046464));
#49027=CARTESIAN_POINT('Ctrl Pts',(168.923242078241,2.42941438769558,330.72145367105));
#49028=CARTESIAN_POINT('Ctrl Pts',(168.915493193213,2.3090784062545,330.655331996425));
#49029=CARTESIAN_POINT('Ctrl Pts',(168.907744308185,2.18625642507057,330.594382460274));
#49030=CARTESIAN_POINT('Ctrl Pts',(168.89998719841,2.06330407936667,330.533368231656));
#49031=CARTESIAN_POINT('Ctrl Pts',(168.892230088635,1.93786081362365,330.477537281851));
#49032=CARTESIAN_POINT('Ctrl Pts',(168.884472978861,1.81040713337798,330.427078715535));
#49033=CARTESIAN_POINT('Ctrl Pts',(168.876711723934,1.68288534596079,330.376593185774));
#49034=CARTESIAN_POINT('Ctrl Pts',(168.868950469008,1.55335137234527,330.331485888366));
#49035=CARTESIAN_POINT('Ctrl Pts',(168.861189214082,1.42230142809693,330.291896166169));
#49036=CARTESIAN_POINT('Ctrl Pts',(168.853415543678,1.29104184664697,330.252243113319));
#49037=CARTESIAN_POINT('Ctrl Pts',(168.845641873273,1.158261827354,330.218125370611));
#49038=CARTESIAN_POINT('Ctrl Pts',(168.837868202868,1.0244692115225,330.189631417745));
#49039=CARTESIAN_POINT('Ctrl Pts',(168.830456398691,0.89690467414496,330.162463865241));
#49040=CARTESIAN_POINT('Ctrl Pts',(168.823044594514,0.768419975064949,330.14040835916));
#49041=CARTESIAN_POINT('Ctrl Pts',(168.815632790337,0.639458215387634,330.123497538884));
#49042=CARTESIAN_POINT('Ctrl Pts',(168.807857711558,0.504175655712586,330.105757868931));
#49043=CARTESIAN_POINT('Ctrl Pts',(168.80008263278,0.367940570799299,330.093623888458));
#49044=CARTESIAN_POINT('Ctrl Pts',(168.792307554001,0.231257167627652,330.087189889186));
#49045=CARTESIAN_POINT('Ctrl Pts',(168.784542042952,0.0947419620855077,
330.080763807359));
#49046=CARTESIAN_POINT('Ctrl Pts',(168.776776531903,-0.0422200773122219,
330.080023768709));
#49047=CARTESIAN_POINT('Ctrl Pts',(168.769011020854,-0.179116752042777,
330.085012690592));
#49048=CARTESIAN_POINT('Ctrl Pts',(168.761253209332,-0.31587769332189,330.089996665945));
#49049=CARTESIAN_POINT('Ctrl Pts',(168.75349539781,-0.452573010809157,330.100698283606));
#49050=CARTESIAN_POINT('Ctrl Pts',(168.745737586288,-0.588687966419104,
330.117108485672));
#49051=CARTESIAN_POINT('Ctrl Pts',(168.737985612765,-0.724700491208062,
330.133506338541));
#49052=CARTESIAN_POINT('Ctrl Pts',(168.730233639242,-0.860133136929075,
330.155604178457));
#49053=CARTESIAN_POINT('Ctrl Pts',(168.722481665719,-0.994474111533304,
330.183340960376));
#49054=CARTESIAN_POINT('Ctrl Pts',(168.714732975161,-1.12875819265524,330.211065995752));
#49055=CARTESIAN_POINT('Ctrl Pts',(168.706984284604,-1.26195114018523,330.244425144507));
#49056=CARTESIAN_POINT('Ctrl Pts',(168.699235594046,-1.39354942775684,330.283305918877));
#49057=CARTESIAN_POINT('Ctrl Pts',(168.691488515668,-1.52512033520574,330.322178603777));
#49058=CARTESIAN_POINT('Ctrl Pts',(168.68374143729,-1.65509686801433,330.366570518525));
#49059=CARTESIAN_POINT('Ctrl Pts',(168.675994358913,-1.7829891707603,330.416318872407));
#49060=CARTESIAN_POINT('Ctrl Pts',(168.668247215607,-1.91088254536701,330.466067643229));
#49061=CARTESIAN_POINT('Ctrl Pts',(168.660500072301,-2.0366912907855,330.521172801024));
#49062=CARTESIAN_POINT('Ctrl Pts',(168.652752928995,-2.15994447135232,330.58142297304));
#49063=CARTESIAN_POINT('Ctrl Pts',(168.645004043967,-2.2832253618506,330.641686690574));
#49064=CARTESIAN_POINT('Ctrl Pts',(168.637255158939,-2.40394919312187,330.707097552424));
#49065=CARTESIAN_POINT('Ctrl Pts',(168.629506273911,-2.52166897991473,330.777397885399));
#49066=CARTESIAN_POINT('Ctrl Pts',(168.621749164136,-2.63951371570567,330.847772835874));
#49067=CARTESIAN_POINT('Ctrl Pts',(168.613992054361,-2.75434770152443,330.923047423733));
#49068=CARTESIAN_POINT('Ctrl Pts',(168.606234944587,-2.86575188609779,331.002919917011));
#49069=CARTESIAN_POINT('Ctrl Pts',(168.59847368966,-2.97721560150531,331.082835091596));
#49070=CARTESIAN_POINT('Ctrl Pts',(168.590712434734,-3.08524555599869,331.167352826612));
#49071=CARTESIAN_POINT('Ctrl Pts',(168.582951179808,-3.18945604248086,331.25613125022));
#49072=CARTESIAN_POINT('Ctrl Pts',(168.575177509403,-3.29383323177945,331.345051690373));
#49073=CARTESIAN_POINT('Ctrl Pts',(168.567403838999,-3.39437845684813,331.438246173079));
#49074=CARTESIAN_POINT('Ctrl Pts',(168.559630168594,-3.49074249114981,331.535335525194));
#49075=CARTESIAN_POINT('Ctrl Pts',(168.552218364417,-3.58262075647029,331.62790534461));
#49076=CARTESIAN_POINT('Ctrl Pts',(168.54480656024,-3.67069814518832,331.72401536928));
#49077=CARTESIAN_POINT('Ctrl Pts',(168.537394756063,-3.75470742271936,331.823310649076));
#49078=CARTESIAN_POINT('Ctrl Pts',(168.529666927997,-3.8422986808223,331.926839672733));
#49079=CARTESIAN_POINT('Ctrl Pts',(168.521939099932,-3.92575403084158,332.034170690932));
#49080=CARTESIAN_POINT('Ctrl Pts',(168.514211271866,-4.00472205233481,332.144937067936));
#49081=CARTESIAN_POINT('Ctrl Pts',(168.506495931509,-4.08356246622131,332.25552445309));
#49082=CARTESIAN_POINT('Ctrl Pts',(168.498780591152,-4.15792976324953,332.369535823212));
#49083=CARTESIAN_POINT('Ctrl Pts',(168.491065250795,-4.22751147335056,332.486570111344));
#49084=CARTESIAN_POINT('Ctrl Pts',(168.483357140694,-4.29702797653107,332.603494723448));
#49085=CARTESIAN_POINT('Ctrl Pts',(168.475649030593,-4.36176761093657,332.723436281665));
#49086=CARTESIAN_POINT('Ctrl Pts',(168.467940920492,-4.42145994481158,332.845963087845));
#49087=CARTESIAN_POINT('Ctrl Pts',(168.460238312771,-4.48110966773853,332.968402429136));
#49088=CARTESIAN_POINT('Ctrl Pts',(168.45253570505,-4.5357190847303,333.093422992699));
#49089=CARTESIAN_POINT('Ctrl Pts',(168.444833097328,-4.58506288522917,333.220567112534));
#49090=CARTESIAN_POINT('Ctrl Pts',(168.437134268494,-4.63438247774049,333.347648855674));
#49091=CARTESIAN_POINT('Ctrl Pts',(168.429435439659,-4.67844145156572,333.476851713406));
#49092=CARTESIAN_POINT('Ctrl Pts',(168.421736610824,-4.71706216808615,333.607697028334));
#49093=CARTESIAN_POINT('Ctrl Pts',(168.414038565493,-4.7556789542093,333.738529027246));
#49094=CARTESIAN_POINT('Ctrl Pts',(168.406340520161,-4.7888584645556,333.871002773357));
#49095=CARTESIAN_POINT('Ctrl Pts',(168.39864247483,-4.8164726598156,334.004623598959));
#49096=CARTESIAN_POINT('Ctrl Pts',(168.390944917703,-4.84408510380512,334.138235950435));
#49097=CARTESIAN_POINT('Ctrl Pts',(168.383247360575,-4.86613286024566,334.272994847622));
#49098=CARTESIAN_POINT('Ctrl Pts',(168.375549803448,-4.88253898479343,334.408395297118));
#49099=CARTESIAN_POINT('Ctrl Pts',(168.36784884037,-4.89895236858437,334.543855657458));
#49100=CARTESIAN_POINT('Ctrl Pts',(168.360147877293,-4.90971909262329,334.679957743058));
#49101=CARTESIAN_POINT('Ctrl Pts',(168.352446914215,-4.91481407985134,334.816191341349));
#49102=CARTESIAN_POINT('Ctrl Pts',(168.34890373498,-4.91715826106239,334.878871820639));
#49103=CARTESIAN_POINT('Ctrl Pts',(168.345360555744,-4.91830252956736,334.941580112913));
#49104=CARTESIAN_POINT('Ctrl Pts',(168.341817376508,-4.91824814939254,335.004266555616));
#49105=CARTESIAN_POINT('',(166.591817376549,-4.91824999464061,335.000229603117));
#49106=CARTESIAN_POINT('Ctrl Pts',(168.341817376469,-4.91824814939194,335.004266556313));
#49107=CARTESIAN_POINT('Ctrl Pts',(168.332452975502,-4.91810442596984,335.169942901091));
#49108=CARTESIAN_POINT('Ctrl Pts',(168.323088574534,-4.90958550624772,335.335252813395));
#49109=CARTESIAN_POINT('Ctrl Pts',(168.313724173567,-4.89282474710446,335.499448752749));
#49110=CARTESIAN_POINT('Ctrl Pts',(168.304233401961,-4.87583780500957,335.665860482084));
#49111=CARTESIAN_POINT('Ctrl Pts',(168.294742630354,-4.85038513728699,335.831127973892));
#49112=CARTESIAN_POINT('Ctrl Pts',(168.285251858748,-4.81665466580062,335.994495295575));
#49113=CARTESIAN_POINT('Ctrl Pts',(168.276553479761,-4.78574038016243,336.144222940162));
#49114=CARTESIAN_POINT('Ctrl Pts',(168.267855100775,-4.74787344150753,336.292354748403));
#49115=CARTESIAN_POINT('Ctrl Pts',(168.259156721789,-4.70323347838745,336.438324688753));
#49116=CARTESIAN_POINT('Ctrl Pts',(168.251381643011,-4.66333187942603,336.568800469044));
#49117=CARTESIAN_POINT('Ctrl Pts',(168.243606564232,-4.61793368071984,336.697820759686));
#49118=CARTESIAN_POINT('Ctrl Pts',(168.235831485454,-4.56716195508446,336.824887596135));
#49119=CARTESIAN_POINT('Ctrl Pts',(168.228065974405,-4.51645270728983,336.951798068753));
#49120=CARTESIAN_POINT('Ctrl Pts',(168.220300463356,-4.46038323312446,337.076759510645));
#49121=CARTESIAN_POINT('Ctrl Pts',(168.212534952307,-4.3991266742254,337.199287968098));
#49122=CARTESIAN_POINT('Ctrl Pts',(168.204777140785,-4.33793085138285,337.321694938227));
#49123=CARTESIAN_POINT('Ctrl Pts',(168.197019329263,-4.2715583523474,337.441673377187));
#49124=CARTESIAN_POINT('Ctrl Pts',(168.18926151774,-4.20023067573399,337.558758553112));
#49125=CARTESIAN_POINT('Ctrl Pts',(168.181509544217,-4.12895667545897,337.675755618729));
#49126=CARTESIAN_POINT('Ctrl Pts',(168.173757570694,-4.05273512239202,337.7898634226));
#49127=CARTESIAN_POINT('Ctrl Pts',(168.166005597171,-3.97183361027012,337.900641452305));
#49128=CARTESIAN_POINT('Ctrl Pts',(168.158256906614,-3.8909663599867,338.011372567448));
#49129=CARTESIAN_POINT('Ctrl Pts',(168.150508216056,-3.80542332268452,338.118776398137));
#49130=CARTESIAN_POINT('Ctrl Pts',(168.142759525498,-3.71551548780974,338.222441267478));
#49131=CARTESIAN_POINT('Ctrl Pts',(168.135012447121,-3.625626359011,338.326084568477));
#49132=CARTESIAN_POINT('Ctrl Pts',(168.127265368743,-3.53137449491998,338.425990160369));
#49133=CARTESIAN_POINT('Ctrl Pts',(168.119518290365,-3.43311100394988,338.521779649135));
#49134=CARTESIAN_POINT('Ctrl Pts',(168.111771147059,-3.33484668943716,338.617569940708));
#49135=CARTESIAN_POINT('Ctrl Pts',(168.104024003753,-3.232570960876,338.709243787506));
#49136=CARTESIAN_POINT('Ctrl Pts',(168.096276860448,-3.12667130480761,338.796460142579));
#49137=CARTESIAN_POINT('Ctrl Pts',(168.088527975419,-3.02074784024828,338.883696105741));
#49138=CARTESIAN_POINT('Ctrl Pts',(168.080779090391,-2.91119912861033,338.966472334594));
#49139=CARTESIAN_POINT('Ctrl Pts',(168.073030205363,-2.79844487379361,339.044488762605));
#49140=CARTESIAN_POINT('Ctrl Pts',(168.065273095589,-2.68557094044573,339.122587998059));
#49141=CARTESIAN_POINT('Ctrl Pts',(168.057515985814,-2.56948498925305,339.195917117869));
#49142=CARTESIAN_POINT('Ctrl Pts',(168.049758876039,-2.45063525086603,339.264219732813));
#49143=CARTESIAN_POINT('Ctrl Pts',(168.041997621113,-2.33172200297893,339.332558846491));
#49144=CARTESIAN_POINT('Ctrl Pts',(168.034236366187,-2.21004237165713,339.395865922884));
#49145=CARTESIAN_POINT('Ctrl Pts',(168.026475111261,-2.0860673061139,339.453931550536));
#49146=CARTESIAN_POINT('Ctrl Pts',(168.018701440856,-1.96189392086918,339.51209006427));
#49147=CARTESIAN_POINT('Ctrl Pts',(168.010927770451,-1.83541812455816,339.564990223423));
#49148=CARTESIAN_POINT('Ctrl Pts',(168.003154100047,-1.70712970206209,339.612471272847));
#49149=CARTESIAN_POINT('Ctrl Pts',(167.995742295869,-1.58481313649632,339.657742067998));
#49150=CARTESIAN_POINT('Ctrl Pts',(167.988330491692,-1.46084917617341,339.69808682958));
#49151=CARTESIAN_POINT('Ctrl Pts',(167.980918687515,-1.33567159055165,339.733409391199));
#49152=CARTESIAN_POINT('Ctrl Pts',(167.973143608737,-1.2043586785751,339.770463216783));
#49153=CARTESIAN_POINT('Ctrl Pts',(167.965368529958,-1.07129519337819,339.802107185413));
#49154=CARTESIAN_POINT('Ctrl Pts',(167.95759345118,-0.93696648573386,339.828175314455));
#49155=CARTESIAN_POINT('Ctrl Pts',(167.949827940131,-0.802803078116049,
339.854211365005));
#49156=CARTESIAN_POINT('Ctrl Pts',(167.942062429082,-0.667377925956069,
339.874685154483));
#49157=CARTESIAN_POINT('Ctrl Pts',(167.934296918033,-0.531191693133408,
339.889480386263));
#49158=CARTESIAN_POINT('Ctrl Pts',(167.926539106511,-0.395140489357063,
339.904260948526));
#49159=CARTESIAN_POINT('Ctrl Pts',(167.918781294988,-0.258330092726615,
339.913374115775));
#49160=CARTESIAN_POINT('Ctrl Pts',(167.911023483466,-0.121271171791649,
339.91675465784));
#49161=CARTESIAN_POINT('Ctrl Pts',(167.903271509943,0.0156846079588316,
339.92013265594));
#49162=CARTESIAN_POINT('Ctrl Pts',(167.89551953642,0.152888150572768,339.917786606029));
#49163=CARTESIAN_POINT('Ctrl Pts',(167.887767562897,0.289824209434218,339.909703146844));
#49164=CARTESIAN_POINT('Ctrl Pts',(167.880018872339,0.426702275793465,339.901623111007));
#49165=CARTESIAN_POINT('Ctrl Pts',(167.872270181782,0.563312694322252,339.887810521575));
#49166=CARTESIAN_POINT('Ctrl Pts',(167.864521491224,0.6991409829054,339.868304114219));
#49167=CARTESIAN_POINT('Ctrl Pts',(167.856774412846,0.834941011278671,339.848801765334));
#49168=CARTESIAN_POINT('Ctrl Pts',(167.849027334469,0.969958846723169,339.823608010398));
#49169=CARTESIAN_POINT('Ctrl Pts',(167.841280256091,1.10368628472728,339.792813333253));
#49170=CARTESIAN_POINT('Ctrl Pts',(167.833533112785,1.23741484349603,339.762018398018));
#49171=CARTESIAN_POINT('Ctrl Pts',(167.825785969479,1.36985260234822,339.72562253466));
#49172=CARTESIAN_POINT('Ctrl Pts',(167.818038826173,1.50050307642865,339.683767028806));
#49173=CARTESIAN_POINT('Ctrl Pts',(167.810289941145,1.63118292350944,339.641902112945));
#49174=CARTESIAN_POINT('Ctrl Pts',(167.802541056117,1.76007431407625,339.594575231341));
#49175=CARTESIAN_POINT('Ctrl Pts',(167.794792171089,1.88669778991771,339.541976938737));
#49176=CARTESIAN_POINT('Ctrl Pts',(167.787035061314,2.01345566522474,339.489322817762));
#49177=CARTESIAN_POINT('Ctrl Pts',(167.779277951539,2.13794045568189,339.431386259172));
#49178=CARTESIAN_POINT('Ctrl Pts',(167.771520841765,2.2596939947986,339.368405442764));
#49179=CARTESIAN_POINT('Ctrl Pts',(167.763759586839,2.38151259511362,339.305390971421));
#49180=CARTESIAN_POINT('Ctrl Pts',(167.755998331912,2.50059669673383,339.237327065117));
#49181=CARTESIAN_POINT('Ctrl Pts',(167.748237076986,2.61651534345585,339.164496430538));
#49182=CARTESIAN_POINT('Ctrl Pts',(167.740463406582,2.73261942223481,339.091549290678));
#49183=CARTESIAN_POINT('Ctrl Pts',(167.732689736177,2.84554760520566,339.013820406845));
#49184=CARTESIAN_POINT('Ctrl Pts',(167.724916065772,2.95489965923097,338.93163465576));
#49185=CARTESIAN_POINT('Ctrl Pts',(167.717504261595,3.05916134883301,338.853274671161));
#49186=CARTESIAN_POINT('Ctrl Pts',(167.710092457418,3.16017213154598,338.770863597745));
#49187=CARTESIAN_POINT('Ctrl Pts',(167.702680653241,3.2576164014527,338.68471416035));
#49188=CARTESIAN_POINT('Ctrl Pts',(167.694905574463,3.35983670529898,338.594342282403));
#49189=CARTESIAN_POINT('Ctrl Pts',(167.687130495684,3.45845508063529,338.499570726072));
#49190=CARTESIAN_POINT('Ctrl Pts',(167.679355416906,3.55306929797189,338.40071781045));
#49191=CARTESIAN_POINT('Ctrl Pts',(167.671589905857,3.6475670864906,338.301986539634));
#49192=CARTESIAN_POINT('Ctrl Pts',(167.663824394808,3.73807025337985,338.199184182286));
#49193=CARTESIAN_POINT('Ctrl Pts',(167.656058883759,3.82421006437014,338.092668822566));
#49194=CARTESIAN_POINT('Ctrl Pts',(167.648301072236,3.91026446748709,337.986259073134));
#49195=CARTESIAN_POINT('Ctrl Pts',(167.640543260714,3.99196388004277,337.876143949598));
#49196=CARTESIAN_POINT('Ctrl Pts',(167.632785449192,4.06897709654346,337.762717584247));
#49197=CARTESIAN_POINT('Ctrl Pts',(167.625033475669,4.14593235815642,337.649376575832));
#49198=CARTESIAN_POINT('Ctrl Pts',(167.617281502146,4.21820822438157,337.532729607516));
#49199=CARTESIAN_POINT('Ctrl Pts',(167.609529528623,4.28551462993841,337.413202730623));
#49200=CARTESIAN_POINT('Ctrl Pts',(167.601780838065,4.35279253119258,337.293726473432));
#49201=CARTESIAN_POINT('Ctrl Pts',(167.594032147508,4.41510496623061,337.171373073328));
#49202=CARTESIAN_POINT('Ctrl Pts',(167.58628345695,4.47220609291166,337.046596131391));
#49203=CARTESIAN_POINT('Ctrl Pts',(167.578536378572,4.52929533922637,336.921845150339));
#49204=CARTESIAN_POINT('Ctrl Pts',(167.570789300194,4.58117527129683,336.794671985621));
#49205=CARTESIAN_POINT('Ctrl Pts',(167.563042221817,4.62764696029223,336.665552963252));
#49206=CARTESIAN_POINT('Ctrl Pts',(167.555295078511,4.67411903876512,336.536432858741));
#49207=CARTESIAN_POINT('Ctrl Pts',(167.547547935205,4.71518265138769,336.40536723183));
#49208=CARTESIAN_POINT('Ctrl Pts',(167.539800791899,4.75068793181425,336.272850044983));
#49209=CARTESIAN_POINT('Ctrl Pts',(167.532051906871,4.78620119458164,336.14030306546));
#49210=CARTESIAN_POINT('Ctrl Pts',(167.524303021843,4.81615353738773,336.006304254103));
#49211=CARTESIAN_POINT('Ctrl Pts',(167.516554136815,4.84044573943344,335.871359917658));
#49212=CARTESIAN_POINT('Ctrl Pts',(167.50879702704,4.8647637254734,335.736272349899));
#49213=CARTESIAN_POINT('Ctrl Pts',(167.501039917265,4.88340950038487,335.600237637585));
#49214=CARTESIAN_POINT('Ctrl Pts',(167.493282807491,4.89633541446301,335.463769955447));
#49215=CARTESIAN_POINT('Ctrl Pts',(167.485521552565,4.90926823573635,335.327229349343));
#49216=CARTESIAN_POINT('Ctrl Pts',(167.477760297638,4.91647508527644,335.190255702535));
#49217=CARTESIAN_POINT('Ctrl Pts',(167.469999042712,4.91796048203675,335.053364404099));
#49218=CARTESIAN_POINT('Ctrl Pts',(167.462225372308,4.91944825494779,334.916254124198));
#49219=CARTESIAN_POINT('Ctrl Pts',(167.454451701903,4.91519629788326,334.779226846796));
#49220=CARTESIAN_POINT('Ctrl Pts',(167.446678031498,4.90526121749234,334.642794945913));
#49221=CARTESIAN_POINT('Ctrl Pts',(167.439266227321,4.89578861748388,334.512713982839));
#49222=CARTESIAN_POINT('Ctrl Pts',(167.431854423144,4.88115011820902,334.383174500114));
#49223=CARTESIAN_POINT('Ctrl Pts',(167.424442618967,4.86143790418352,334.25461113084));
#49224=CARTESIAN_POINT('Ctrl Pts',(167.416667540189,4.84075953582891,334.119746487866));
#49225=CARTESIAN_POINT('Ctrl Pts',(167.40889246141,4.81443217386325,333.985529864994));
#49226=CARTESIAN_POINT('Ctrl Pts',(167.401117382632,4.78250583014581,333.852471766308));
#49227=CARTESIAN_POINT('Ctrl Pts',(167.393351871583,4.75061877382685,333.719577404083));
#49228=CARTESIAN_POINT('Ctrl Pts',(167.385586360534,4.71314653501564,333.587839105886));
#49229=CARTESIAN_POINT('Ctrl Pts',(167.377820849485,4.67019069104927,333.457760728117));
#49230=CARTESIAN_POINT('Ctrl Pts',(167.370063037962,4.62727743792727,333.327811323439));
#49231=CARTESIAN_POINT('Ctrl Pts',(167.36230522644,4.57889152138716,333.19951893269));
#49232=CARTESIAN_POINT('Ctrl Pts',(167.354547414918,4.5251851413841,333.073375361235));
#49233=CARTESIAN_POINT('Ctrl Pts',(167.346795441395,4.47151917713512,332.947326716817));
#49234=CARTESIAN_POINT('Ctrl Pts',(167.339043467872,4.41254087132668,332.823424031213));
#49235=CARTESIAN_POINT('Ctrl Pts',(167.331291494349,4.3484515286403,332.702141787323));
#49236=CARTESIAN_POINT('Ctrl Pts',(167.323542803791,4.28438932782858,332.580910906536));
#49237=CARTESIAN_POINT('Ctrl Pts',(167.315794113234,4.21522057747143,332.462298605102));
#49238=CARTESIAN_POINT('Ctrl Pts',(167.308045422676,4.14119368110637,332.346757086495));
#49239=CARTESIAN_POINT('Ctrl Pts',(167.300298344298,4.0671821866554,332.231239607266));
#49240=CARTESIAN_POINT('Ctrl Pts',(167.292551265921,3.9883147674373,332.118791968955));
#49241=CARTESIAN_POINT('Ctrl Pts',(167.284804187543,3.90488432435392,332.009839222397));
#49242=CARTESIAN_POINT('Ctrl Pts',(167.277057044237,3.82145318204311,331.90088556271));
#49243=CARTESIAN_POINT('Ctrl Pts',(167.269309900931,3.73345917723024,331.795427163536));
#49244=CARTESIAN_POINT('Ctrl Pts',(167.261562757625,3.64123659221255,331.693857362116));
#49245=CARTESIAN_POINT('Ctrl Pts',(167.253813872597,3.54899327359987,331.592264725649));
#49246=CARTESIAN_POINT('Ctrl Pts',(167.246064987569,3.45251974574801,331.494562715903));
#49247=CARTESIAN_POINT('Ctrl Pts',(167.238316102541,3.35218807873302,331.401108761396));
#49248=CARTESIAN_POINT('Ctrl Pts',(167.230558992766,3.25174991864996,331.307555613896));
#49249=CARTESIAN_POINT('Ctrl Pts',(167.222801882992,3.1474457255907,331.21825979548));
#49250=CARTESIAN_POINT('Ctrl Pts',(167.215044773217,3.039682094067,331.13353962525));
#49251=CARTESIAN_POINT('Ctrl Pts',(167.207283518291,2.93186087710422,331.048774183271));
#49252=CARTESIAN_POINT('Ctrl Pts',(167.199522263364,2.82057685511416,330.968589489907));
#49253=CARTESIAN_POINT('Ctrl Pts',(167.191761008438,2.70626587523024,330.893260651677));
#49254=CARTESIAN_POINT('Ctrl Pts',(167.183987338034,2.59177203503238,330.817811311855));
#49255=CARTESIAN_POINT('Ctrl Pts',(167.176213667629,2.4742418961718,330.747233550837));
#49256=CARTESIAN_POINT('Ctrl Pts',(167.168439997224,2.35413695799786,330.681757041864));
#49257=CARTESIAN_POINT('Ctrl Pts',(167.161028193047,2.23962293359131,330.619328480137));
#49258=CARTESIAN_POINT('Ctrl Pts',(167.15361638887,2.12276868704919,330.561537059399));
#49259=CARTESIAN_POINT('Ctrl Pts',(167.146204584693,2.00398959695076,330.508540464636));
#49260=CARTESIAN_POINT('Ctrl Pts',(167.138429505915,1.87938878982209,330.452946348894));
#49261=CARTESIAN_POINT('Ctrl Pts',(167.130654427136,1.75227592203912,330.402453273256));
#49262=CARTESIAN_POINT('Ctrl Pts',(167.122879348358,1.62310735166507,330.357295444736));
#49263=CARTESIAN_POINT('Ctrl Pts',(167.115113837309,1.49409773144018,330.312193185798));
#49264=CARTESIAN_POINT('Ctrl Pts',(167.10734832626,1.36303780739623,330.272413238554));
#49265=CARTESIAN_POINT('Ctrl Pts',(167.099582815211,1.23040625245394,330.238142850061));
#49266=CARTESIAN_POINT('Ctrl Pts',(167.091825003689,1.09790620208455,330.203906440759));
#49267=CARTESIAN_POINT('Ctrl Pts',(167.084067192166,0.963837997882614,330.175168816196));
#49268=CARTESIAN_POINT('Ctrl Pts',(167.076309380644,0.828697573599784,330.152068132285));
#49269=CARTESIAN_POINT('Ctrl Pts',(167.068557407121,0.693658846771776,330.128984832371));
#49270=CARTESIAN_POINT('Ctrl Pts',(167.060805433598,0.557549889651754,330.111530095257));
#49271=CARTESIAN_POINT('Ctrl Pts',(167.053053460075,0.420878642548264,330.099791409466));
#49272=CARTESIAN_POINT('Ctrl Pts',(167.045304769518,0.284265275799041,330.088057695015));
#49273=CARTESIAN_POINT('Ctrl Pts',(167.03755607896,0.147090481320391,330.082035250562));
#49274=CARTESIAN_POINT('Ctrl Pts',(167.029807388402,0.00986895206824741,
330.081759901521));
#49275=CARTESIAN_POINT('Ctrl Pts',(167.022060310024,-0.127324027098686,
330.081484609769));
#49276=CARTESIAN_POINT('Ctrl Pts',(167.014313231647,-0.264563331070165,
330.086954035818));
#49277=CARTESIAN_POINT('Ctrl Pts',(167.006566153269,-0.401333020046105,
330.098151892447));
#49278=CARTESIAN_POINT('Ctrl Pts',(166.998819009963,-0.538103855283608,
330.109349842925));
#49279=CARTESIAN_POINT('Ctrl Pts',(166.991071866657,-0.674404678104511,
330.126276287847));
#49280=CARTESIAN_POINT('Ctrl Pts',(166.983324723351,-0.809723823498836,
330.148862979449));
#49281=CARTESIAN_POINT('Ctrl Pts',(166.975575838323,-0.945073391509929,
330.171454749019));
#49282=CARTESIAN_POINT('Ctrl Pts',(166.967826953295,-1.07944045745707,330.199709233148));
#49283=CARTESIAN_POINT('Ctrl Pts',(166.960078068267,-1.21232310360615,330.233506975253));
#49284=CARTESIAN_POINT('Ctrl Pts',(166.952320958492,-1.34534679276888,330.26734059063));
#49285=CARTESIAN_POINT('Ctrl Pts',(166.944563848718,-1.4768825353558,330.306729120668));
#49286=CARTESIAN_POINT('Ctrl Pts',(166.936806738943,-1.60644261842071,330.351502912099));
#49287=CARTESIAN_POINT('Ctrl Pts',(166.929045484017,-1.73607193425144,330.396300629213));
#49288=CARTESIAN_POINT('Ctrl Pts',(166.921284229091,-1.86372312334087,330.446489198869));
#49289=CARTESIAN_POINT('Ctrl Pts',(166.913522974164,-1.98892898085688,330.501850983837));
#49290=CARTESIAN_POINT('Ctrl Pts',(166.90574930376,-2.1143351269404,330.557301329619));
#49291=CARTESIAN_POINT('Ctrl Pts',(166.897975633355,-2.23728777390671,330.617941254544));
#49292=CARTESIAN_POINT('Ctrl Pts',(166.89020196295,-2.35734404084748,330.683506963335));
#49293=CARTESIAN_POINT('Ctrl Pts',(166.882790158773,-2.47181165967819,330.746020572607));
#49294=CARTESIAN_POINT('Ctrl Pts',(166.875378354596,-2.58364623620141,330.813011547668));
#49295=CARTESIAN_POINT('Ctrl Pts',(166.867966550419,-2.69249038456561,330.884215920202));
#49296=CARTESIAN_POINT('Ctrl Pts',(166.860201822508,-2.80651730386932,330.95881079152));
#49297=CARTESIAN_POINT('Ctrl Pts',(166.852437094596,-2.91762449540572,331.038267340492));
#49298=CARTESIAN_POINT('Ctrl Pts',(166.844672366685,-3.02536873599656,331.122329684752));
#49299=CARTESIAN_POINT('Ctrl Pts',(166.836917201062,-3.13298028919917,331.206288505957));
#49300=CARTESIAN_POINT('Ctrl Pts',(166.829162035438,-3.23723682527444,331.294841598457));
#49301=CARTESIAN_POINT('Ctrl Pts',(166.821406869815,-3.33772247606863,331.387688865111));
#49302=CARTESIAN_POINT('Ctrl Pts',(166.81365938716,-3.4381085766876,331.480444148864));
#49303=CARTESIAN_POINT('Ctrl Pts',(166.805911904505,-3.53473093998224,331.577484876766));
#49304=CARTESIAN_POINT('Ctrl Pts',(166.798164421851,-3.62720559656636,331.678469837148));
#49305=CARTESIAN_POINT('Ctrl Pts',(166.790422749604,-3.71961089959684,331.779379061472));
#49306=CARTESIAN_POINT('Ctrl Pts',(166.782681077357,-3.80787442356198,331.88422634268));
#49307=CARTESIAN_POINT('Ctrl Pts',(166.774939405109,-3.89164828173828,331.992632926671));
#49308=CARTESIAN_POINT('Ctrl Pts',(166.767200970691,-3.97538710285986,332.10099417137));
#49309=CARTESIAN_POINT('Ctrl Pts',(166.759462536272,-4.05463975335757,332.212911448724));
#49310=CARTESIAN_POINT('Ctrl Pts',(166.751724101854,-4.12909812191281,332.327972350046));
#49311=CARTESIAN_POINT('Ctrl Pts',(166.743987234331,-4.20354141396952,332.443009953578));
#49312=CARTESIAN_POINT('Ctrl Pts',(166.736250366808,-4.27319214202715,332.561189586087));
#49313=CARTESIAN_POINT('Ctrl Pts',(166.728513499286,-4.33778533951076,332.682069584559));
#49314=CARTESIAN_POINT('Ctrl Pts',(166.720776511659,-4.4023795397099,332.802951459517));
#49315=CARTESIAN_POINT('Ctrl Pts',(166.713039524033,-4.46191586819535,332.926533438142));
#49316=CARTESIAN_POINT('Ctrl Pts',(166.705302536406,-4.51617537083237,333.052349342827));
#49317=CARTESIAN_POINT('Ctrl Pts',(166.697563741948,-4.57044754478014,333.178194629507));
#49318=CARTESIAN_POINT('Ctrl Pts',(166.68982494749,-4.61944028570309,333.306274520356));
#49319=CARTESIAN_POINT('Ctrl Pts',(166.682086153033,-4.66298298548585,333.436103347542));
#49320=CARTESIAN_POINT('Ctrl Pts',(166.674339136885,-4.70657194500147,333.566070104781));
#49321=CARTESIAN_POINT('Ctrl Pts',(166.666592120738,-4.74469917321079,333.697789137461));
#49322=CARTESIAN_POINT('Ctrl Pts',(166.65884510459,-4.77724397403381,333.830759616222));
#49323=CARTESIAN_POINT('Ctrl Pts',(166.651093865666,-4.80980651451597,333.9638025751));
#49324=CARTESIAN_POINT('Ctrl Pts',(166.643342626742,-4.83678048788805,334.098097955067));
#49325=CARTESIAN_POINT('Ctrl Pts',(166.635591387817,-4.85809665151938,334.233136265692));
#49326=CARTESIAN_POINT('Ctrl Pts',(166.627827928584,-4.87944642140552,334.368387472595));
#49327=CARTESIAN_POINT('Ctrl Pts',(166.620064469351,-4.89512051445102,334.504383560939));
#49328=CARTESIAN_POINT('Ctrl Pts',(166.612301010117,-4.90510166638276,334.640610649923));
#49329=CARTESIAN_POINT('Ctrl Pts',(166.605473132261,-4.91387998081784,334.760420891251));
#49330=CARTESIAN_POINT('Ctrl Pts',(166.598645254405,-4.91825558830559,334.880409615298));
#49331=CARTESIAN_POINT('Ctrl Pts',(166.591817376549,-4.91824999464062,335.000229603117));
#49332=CARTESIAN_POINT('',(164.841817376508,-4.91683592588205,334.995612015269));
#49333=CARTESIAN_POINT('Ctrl Pts',(166.591817376508,-4.91824999464058,335.000229603829));
#49334=CARTESIAN_POINT('Ctrl Pts',(166.591121089721,-4.91824942421341,335.012448491774));
#49335=CARTESIAN_POINT('Ctrl Pts',(166.590424802933,-4.91820331902207,335.02466725531));
#49336=CARTESIAN_POINT('Ctrl Pts',(166.589728516146,-4.91811168125916,335.036885676925));
#49337=CARTESIAN_POINT('Ctrl Pts',(166.581953437367,-4.91708840918464,335.173322547882));
#49338=CARTESIAN_POINT('Ctrl Pts',(166.574178358589,-4.91038172830435,335.30993240212));
#49339=CARTESIAN_POINT('Ctrl Pts',(166.56640327981,-4.89796754502857,335.446202857843));
#49340=CARTESIAN_POINT('Ctrl Pts',(166.558637768761,-4.88556863819563,335.582305624094));
#49341=CARTESIAN_POINT('Ctrl Pts',(166.550872257712,-4.86747623873167,335.718069437295));
#49342=CARTESIAN_POINT('Ctrl Pts',(166.543106746663,-4.84371823824118,335.852981061355));
#49343=CARTESIAN_POINT('Ctrl Pts',(166.535348935141,-4.81998379387741,335.987758920146));
#49344=CARTESIAN_POINT('Ctrl Pts',(166.527591123619,-4.79059499490334,336.121685888821));
#49345=CARTESIAN_POINT('Ctrl Pts',(166.519833312096,-4.75563156393336,336.25425335982));
#49346=CARTESIAN_POINT('Ctrl Pts',(166.512081338573,-4.72069444405382,336.386721069595));
#49347=CARTESIAN_POINT('Ctrl Pts',(166.50432936505,-4.68019114157413,336.517830941627));
#49348=CARTESIAN_POINT('Ctrl Pts',(166.496577391527,-4.634252467892,336.647084432061));
#49349=CARTESIAN_POINT('Ctrl Pts',(166.488828700969,-4.58833324926552,336.776283183564));
#49350=CARTESIAN_POINT('Ctrl Pts',(166.481080010412,-4.53698336834799,336.903626749586));
#49351=CARTESIAN_POINT('Ctrl Pts',(166.473331319854,-4.48038345488503,337.028631844296));
#49352=CARTESIAN_POINT('Ctrl Pts',(166.465584241476,-4.42379531750681,337.153610930652));
#49353=CARTESIAN_POINT('Ctrl Pts',(166.457837163098,-4.36195948139403,337.276252157603));
#49354=CARTESIAN_POINT('Ctrl Pts',(166.450090084721,-4.29510452273087,337.396092694642));
#49355=CARTESIAN_POINT('Ctrl Pts',(166.442342941415,-4.22824900375874,337.51593423606));
#49356=CARTESIAN_POINT('Ctrl Pts',(166.434595798109,-4.15637446876197,337.632974699398));
#49357=CARTESIAN_POINT('Ctrl Pts',(166.426848654803,-4.07975501434121,337.74677667193));
#49358=CARTESIAN_POINT('Ctrl Pts',(166.419099769775,-4.0031183342405,337.860604229561));
#49359=CARTESIAN_POINT('Ctrl Pts',(166.411350884747,-3.92173483024071,337.971191523412));
#49360=CARTESIAN_POINT('Ctrl Pts',(166.403601999719,-3.83592116794736,338.078131227838));
#49361=CARTESIAN_POINT('Ctrl Pts',(166.395844889944,-3.75001642214616,338.185184439172));
#49362=CARTESIAN_POINT('Ctrl Pts',(166.388087780169,-3.65967236995282,338.288582021879));
#49363=CARTESIAN_POINT('Ctrl Pts',(166.380330670395,-3.56524547805433,338.387950375037));
#49364=CARTESIAN_POINT('Ctrl Pts',(166.372569415468,-3.47076812744394,338.487371827466));
#49365=CARTESIAN_POINT('Ctrl Pts',(166.364808160542,-3.37220387055343,338.582759488427));
#49366=CARTESIAN_POINT('Ctrl Pts',(166.357046905616,-3.26994434981216,338.673778301916));
#49367=CARTESIAN_POINT('Ctrl Pts',(166.349273235211,-3.16752124716408,338.764942715844));
#49368=CARTESIAN_POINT('Ctrl Pts',(166.341499564807,-3.06139137105344,338.851724069185));
#49369=CARTESIAN_POINT('Ctrl Pts',(166.333725894402,-2.95197829692954,338.933828567307));
#49370=CARTESIAN_POINT('Ctrl Pts',(166.326314090225,-2.84765842772994,339.012111081287));
#49371=CARTESIAN_POINT('Ctrl Pts',(166.318902286048,-2.74035438432368,339.086142193086));
#49372=CARTESIAN_POINT('Ctrl Pts',(166.311490481871,-2.63045447927052,339.155705992366));
#49373=CARTESIAN_POINT('Ctrl Pts',(166.303715403093,-2.51516805249525,339.228679320669));
#49374=CARTESIAN_POINT('Ctrl Pts',(166.295940324314,-2.39666054176947,339.296966960436));
#49375=CARTESIAN_POINT('Ctrl Pts',(166.288165245536,-2.27534978145381,339.360271371662));
#49376=CARTESIAN_POINT('Ctrl Pts',(166.280399734487,-2.15418830175171,339.423497882781));
#49377=CARTESIAN_POINT('Ctrl Pts',(166.272634223438,-2.03023077934567,339.481753187536));
#49378=CARTESIAN_POINT('Ctrl Pts',(166.264868712389,-1.90392389916115,339.534782999075));
#49379=CARTESIAN_POINT('Ctrl Pts',(166.257110900866,-1.77774225261596,339.587760231402));
#49380=CARTESIAN_POINT('Ctrl Pts',(166.249353089344,-1.64921624199713,339.63552213084));
#49381=CARTESIAN_POINT('Ctrl Pts',(166.241595277822,-1.51881670873112,339.677860501103));
#49382=CARTESIAN_POINT('Ctrl Pts',(166.233843304299,-1.38851530524917,339.7201670104));
#49383=CARTESIAN_POINT('Ctrl Pts',(166.226091330776,-1.25634355570021,339.757057994084));
#49384=CARTESIAN_POINT('Ctrl Pts',(166.218339357253,-1.12279148580239,339.788373663564));
#49385=CARTESIAN_POINT('Ctrl Pts',(166.210590666695,-0.989295975285546,
339.819676070839));
#49386=CARTESIAN_POINT('Ctrl Pts',(166.202841976138,-0.854421686841869,
339.84540777102));
#49387=CARTESIAN_POINT('Ctrl Pts',(166.19509328558,-0.718672774956675,339.865459125821));
#49388=CARTESIAN_POINT('Ctrl Pts',(166.187346207202,-0.582952106766372,
339.88550630877));
#49389=CARTESIAN_POINT('Ctrl Pts',(166.179599128824,-0.44635756352715,339.899875440029));
#49390=CARTESIAN_POINT('Ctrl Pts',(166.171852050447,-0.309402044975992,
339.908508270041));
#49391=CARTESIAN_POINT('Ctrl Pts',(166.164104907141,-0.172445378605723,
339.917141172405));
#49392=CARTESIAN_POINT('Ctrl Pts',(166.156357763835,-0.0351281209893634,
339.920037653043));
#49393=CARTESIAN_POINT('Ctrl Pts',(166.148610620529,0.102033568781341,339.917191496509));
#49394=CARTESIAN_POINT('Ctrl Pts',(166.140861735501,0.239226095411862,339.914344700099));
#49395=CARTESIAN_POINT('Ctrl Pts',(166.133112850473,0.376262593886676,339.905752705545));
#49396=CARTESIAN_POINT('Ctrl Pts',(166.125363965445,0.512629169451043,339.891461376432));
#49397=CARTESIAN_POINT('Ctrl Pts',(166.11760685567,0.649140485907691,339.877154878355));
#49398=CARTESIAN_POINT('Ctrl Pts',(166.109849745896,0.784980069679347,339.857137002415));
#49399=CARTESIAN_POINT('Ctrl Pts',(166.102092636121,0.919640847200704,339.831505332157));
#49400=CARTESIAN_POINT('Ctrl Pts',(166.094331381195,1.05437358313591,339.805859965154));
#49401=CARTESIAN_POINT('Ctrl Pts',(166.086570126268,1.18792587726423,339.774594915447));
#49402=CARTESIAN_POINT('Ctrl Pts',(166.078808871342,1.31980403365141,339.737858205482));
#49403=CARTESIAN_POINT('Ctrl Pts',(166.071035200938,1.45189315210982,339.701062728754));
#49404=CARTESIAN_POINT('Ctrl Pts',(166.063261530533,1.58230240922778,339.658778221557));
#49405=CARTESIAN_POINT('Ctrl Pts',(166.055487860128,1.71055552584989,339.611201888389));
#49406=CARTESIAN_POINT('Ctrl Pts',(166.048076055951,1.83283842903757,339.565840244977));
#49407=CARTESIAN_POINT('Ctrl Pts',(166.040664251774,1.95316114532687,339.515668468144));
#49408=CARTESIAN_POINT('Ctrl Pts',(166.033252447597,2.07113197290002,339.460896256733));
#49409=CARTESIAN_POINT('Ctrl Pts',(166.025477368819,2.19488490214934,339.403439496082));
#49410=CARTESIAN_POINT('Ctrl Pts',(166.01770229004,2.31644064929564,339.340738362288));
#49411=CARTESIAN_POINT('Ctrl Pts',(166.009927211262,2.4353228924535,339.272983205208));
#49412=CARTESIAN_POINT('Ctrl Pts',(166.002161700213,2.55405884344275,339.205311425163));
#49413=CARTESIAN_POINT('Ctrl Pts',(165.994396189164,2.67012750008897,339.132598188145));
#49414=CARTESIAN_POINT('Ctrl Pts',(165.986630678115,2.78307330030879,339.055081511833));
#49415=CARTESIAN_POINT('Ctrl Pts',(165.978872866592,2.89590711443881,338.977641693531));
#49416=CARTESIAN_POINT('Ctrl Pts',(165.97111505507,3.00562391379816,338.895408133582));
#49417=CARTESIAN_POINT('Ctrl Pts',(165.963357243548,3.11179382237577,338.808664105631));
#49418=CARTESIAN_POINT('Ctrl Pts',(165.955605270025,3.21788383473024,338.721985355312));
#49419=CARTESIAN_POINT('Ctrl Pts',(165.947853296502,3.32043196763917,338.630803139432));
#49420=CARTESIAN_POINT('Ctrl Pts',(165.940101322979,3.41903867043276,338.535443060295));
#49421=CARTESIAN_POINT('Ctrl Pts',(165.932352632421,3.51760361322926,338.440123366207));
#49422=CARTESIAN_POINT('Ctrl Pts',(165.924603941864,3.61223016543565,338.340629599091));
#49423=CARTESIAN_POINT('Ctrl Pts',(165.916855251306,3.70255330295679,338.23732638164));
#49424=CARTESIAN_POINT('Ctrl Pts',(165.909108172928,3.79285764799476,338.134044657286));
#49425=CARTESIAN_POINT('Ctrl Pts',(165.901361094551,3.87886010216198,338.026955353184));
#49426=CARTESIAN_POINT('Ctrl Pts',(165.893614016173,3.96023412268692,337.916458255488));
#49427=CARTESIAN_POINT('Ctrl Pts',(165.885866872867,4.0416088252045,337.80596023172));
#49428=CARTESIAN_POINT('Ctrl Pts',(165.878119729561,4.11835478492542,337.692054672129));
#49429=CARTESIAN_POINT('Ctrl Pts',(165.870372586255,4.19018745184681,337.575172262371));
#49430=CARTESIAN_POINT('Ctrl Pts',(165.862623701227,4.26203626827674,337.458263574966));
#49431=CARTESIAN_POINT('Ctrl Pts',(165.854874816199,4.32896938923169,337.338377038592));
#49432=CARTESIAN_POINT('Ctrl Pts',(165.847125931171,4.39074728443907,337.215969617727));
#49433=CARTESIAN_POINT('Ctrl Pts',(165.839368821396,4.45259075134274,337.093432272362));
#49434=CARTESIAN_POINT('Ctrl Pts',(165.831611711622,4.50926788565456,336.968369047061));
#49435=CARTESIAN_POINT('Ctrl Pts',(165.823854601847,4.56058634085738,336.84125915886));
#49436=CARTESIAN_POINT('Ctrl Pts',(165.816093346921,4.6119322190018,336.714081347199));
#49437=CARTESIAN_POINT('Ctrl Pts',(165.808332091994,4.65791358127521,336.584855061469));
#49438=CARTESIAN_POINT('Ctrl Pts',(165.800570837068,4.69838773571041,336.454075564552));
#49439=CARTESIAN_POINT('Ctrl Pts',(165.792797166664,4.73892663560221,336.32308686306));
#49440=CARTESIAN_POINT('Ctrl Pts',(165.785023496259,4.77394062330796,336.190540363461));
#49441=CARTESIAN_POINT('Ctrl Pts',(165.777249825854,4.80333779031722,336.056943297727));
#49442=CARTESIAN_POINT('Ctrl Pts',(165.769838021677,4.83136651212972,335.929565207544));
#49443=CARTESIAN_POINT('Ctrl Pts',(165.7624262175,4.85428952052309,335.801232441144));
#49444=CARTESIAN_POINT('Ctrl Pts',(165.755014413323,4.87207118339821,335.672387869017));
#49445=CARTESIAN_POINT('Ctrl Pts',(165.747239334545,4.89072437853965,335.537228240602));
#49446=CARTESIAN_POINT('Ctrl Pts',(165.739464255766,4.90377844711013,335.401078238262));
#49447=CARTESIAN_POINT('Ctrl Pts',(165.731689176988,4.91113569326316,335.264441420463));
#49448=CARTESIAN_POINT('Ctrl Pts',(165.723923665939,4.91848388585642,335.127972742967));
#49449=CARTESIAN_POINT('Ctrl Pts',(165.71615815489,4.92014918370908,334.991018828542));
#49450=CARTESIAN_POINT('Ctrl Pts',(165.708392643841,4.91608521017967,334.854091574086));
#49451=CARTESIAN_POINT('Ctrl Pts',(165.700634832318,4.91202526609185,334.717300083401));
#49452=CARTESIAN_POINT('Ctrl Pts',(165.692877020796,4.90224736683704,334.580535588265));
#49453=CARTESIAN_POINT('Ctrl Pts',(165.685119209274,4.88675709268995,334.444312876211));
#49454=CARTESIAN_POINT('Ctrl Pts',(165.677367235751,4.87127847546538,334.308192676068));
#49455=CARTESIAN_POINT('Ctrl Pts',(165.669615262228,4.85009608377183,334.172613834289));
#49456=CARTESIAN_POINT('Ctrl Pts',(165.661863288705,4.82326750374017,334.038088543646));
#49457=CARTESIAN_POINT('Ctrl Pts',(165.654114598147,4.79645028562807,333.903620224545));
#49458=CARTESIAN_POINT('Ctrl Pts',(165.64636590759,4.76399171132292,333.770204951688));
#49459=CARTESIAN_POINT('Ctrl Pts',(165.638617217032,4.7260008643441,333.638346999886));
#49460=CARTESIAN_POINT('Ctrl Pts',(165.630870138654,4.68801792167829,333.506516482233));
#49461=CARTESIAN_POINT('Ctrl Pts',(165.623123060276,4.64450510397834,333.376243016509));
#49462=CARTESIAN_POINT('Ctrl Pts',(165.615375981899,4.59562188891985,333.248017546726));
#49463=CARTESIAN_POINT('Ctrl Pts',(165.607628838593,4.54673826417296,333.119791002289));
#49464=CARTESIAN_POINT('Ctrl Pts',(165.599881695287,4.49248429153102,332.993612853262));
#49465=CARTESIAN_POINT('Ctrl Pts',(165.592134551981,4.43306815741772,332.869955452534));
#49466=CARTESIAN_POINT('Ctrl Pts',(165.584385666953,4.37363866529608,332.746270250997));
#49467=CARTESIAN_POINT('Ctrl Pts',(165.576636781925,4.30904487156203,332.62510727771));
#49468=CARTESIAN_POINT('Ctrl Pts',(165.568887896897,4.23954142382082,332.506915248491));
#49469=CARTESIAN_POINT('Ctrl Pts',(165.561130787122,4.16996420440202,332.38859776903));
#49470=CARTESIAN_POINT('Ctrl Pts',(165.553373677348,4.09546711964909,332.273257870297));
#49471=CARTESIAN_POINT('Ctrl Pts',(165.545616567573,4.01634906365282,332.161316632417));
#49472=CARTESIAN_POINT('Ctrl Pts',(165.537855312647,3.93718872949713,332.049315576718));
#49473=CARTESIAN_POINT('Ctrl Pts',(165.53009405772,3.85340274244102,331.940717110001));
#49474=CARTESIAN_POINT('Ctrl Pts',(165.522332802794,3.7653303607965,331.835909240151));
#49475=CARTESIAN_POINT('Ctrl Pts',(165.51455913239,3.67711709204406,331.730933711865));
#49476=CARTESIAN_POINT('Ctrl Pts',(165.506785461985,3.58460399062556,331.629761186163));
#49477=CARTESIAN_POINT('Ctrl Pts',(165.49901179158,3.48816786175894,331.532743443197));
#49478=CARTESIAN_POINT('Ctrl Pts',(165.491599987403,3.39622085789249,331.440241899508));
#49479=CARTESIAN_POINT('Ctrl Pts',(165.484188183226,3.30070805193071,331.351517229077));
#49480=CARTESIAN_POINT('Ctrl Pts',(165.476776379049,3.20198258054458,331.266839058333));
#49481=CARTESIAN_POINT('Ctrl Pts',(165.469001300271,3.09841827971757,331.178010558197));
#49482=CARTESIAN_POINT('Ctrl Pts',(165.461226221492,2.99099114366286,331.093354534888));
#49483=CARTESIAN_POINT('Ctrl Pts',(165.453451142714,2.88007175660924,331.013225647308));
#49484=CARTESIAN_POINT('Ctrl Pts',(165.445685631665,2.76928886292286,330.933195363426));
#49485=CARTESIAN_POINT('Ctrl Pts',(165.437920120616,2.65502258272237,330.857681357425));
#49486=CARTESIAN_POINT('Ctrl Pts',(165.430154609567,2.53767828396757,330.786999645196));
#49487=CARTESIAN_POINT('Ctrl Pts',(165.422396798045,2.42045033242669,330.716388014091));
#49488=CARTESIAN_POINT('Ctrl Pts',(165.414638986523,2.30015076838236,330.650599342314));
#49489=CARTESIAN_POINT('Ctrl Pts',(165.406881175,2.17721550745935,330.589907518364));
#49490=CARTESIAN_POINT('Ctrl Pts',(165.399129201477,2.05437275921865,330.529261366937));
#49491=CARTESIAN_POINT('Ctrl Pts',(165.391377227954,1.92889861112814,330.47370460122));
#49492=CARTESIAN_POINT('Ctrl Pts',(165.383625254431,1.80125494017703,330.423465972705));
#49493=CARTESIAN_POINT('Ctrl Pts',(165.375876563874,1.67366532639633,330.373248620279));
#49494=CARTESIAN_POINT('Ctrl Pts',(165.368127873316,1.54390838013171,330.328345068376));
#49495=CARTESIAN_POINT('Ctrl Pts',(165.360379182759,1.41246718818142,330.288936478372));
#49496=CARTESIAN_POINT('Ctrl Pts',(165.352632104381,1.28105334366896,330.249536087655));
#49497=CARTESIAN_POINT('Ctrl Pts',(165.344885026003,1.14795632465699,330.215628496971));
#49498=CARTESIAN_POINT('Ctrl Pts',(165.337137947625,1.0136752789592,330.187345276116));
#49499=CARTESIAN_POINT('Ctrl Pts',(165.329390804319,0.879393107857031,330.15906181822));
#49500=CARTESIAN_POINT('Ctrl Pts',(165.321643661014,0.743927272758503,330.136402904733));
#49501=CARTESIAN_POINT('Ctrl Pts',(165.313896517708,0.607787646905678,330.119449084502));
#49502=CARTESIAN_POINT('Ctrl Pts',(165.30614763268,0.471617413974657,330.102491452693));
#49503=CARTESIAN_POINT('Ctrl Pts',(165.298398747652,0.334773476658537,330.091241514716));
#49504=CARTESIAN_POINT('Ctrl Pts',(165.290649862624,0.197770974091667,330.085727957845));
#49505=CARTESIAN_POINT('Ctrl Pts',(165.282892752849,0.0606230556530012,
330.080208548827));
#49506=CARTESIAN_POINT('Ctrl Pts',(165.275135643074,-0.0766833730620175,
330.080437699315));
#49507=CARTESIAN_POINT('Ctrl Pts',(165.267378533299,-0.213632468050133,
330.086391933508));
#49508=CARTESIAN_POINT('Ctrl Pts',(165.259617278373,-0.350654744255804,
330.092349349453));
#49509=CARTESIAN_POINT('Ctrl Pts',(165.251856023447,-0.487318916999135,
330.104037911745));
#49510=CARTESIAN_POINT('Ctrl Pts',(165.244094768521,-0.623115110034368,
330.121382304162));
#49511=CARTESIAN_POINT('Ctrl Pts',(165.236321098116,-0.759128532722581,
330.138754441953));
#49512=CARTESIAN_POINT('Ctrl Pts',(165.228547427712,-0.894270815584662,
330.161800423681));
#49513=CARTESIAN_POINT('Ctrl Pts',(165.220773757307,-1.02804222826113,330.190393754224));
#49514=CARTESIAN_POINT('Ctrl Pts',(165.21336195313,-1.15558654949415,330.21765605835));
#49515=CARTESIAN_POINT('Ctrl Pts',(165.205950148953,-1.281884477547,330.24996080437));
#49516=CARTESIAN_POINT('Ctrl Pts',(165.198538344776,-1.40651817528927,330.287156942452));
#49517=CARTESIAN_POINT('Ctrl Pts',(165.190763265997,-1.5372605418223,330.326176174063));
#49518=CARTESIAN_POINT('Ctrl Pts',(165.182988187219,-1.66658458536666,330.370701712855));
#49519=CARTESIAN_POINT('Ctrl Pts',(165.17521310844,-1.79399152129524,330.420613852925));
#49520=CARTESIAN_POINT('Ctrl Pts',(165.167447597391,-1.92124167487801,330.47046457293));
#49521=CARTESIAN_POINT('Ctrl Pts',(165.159682086342,-2.04657905435909,330.525688564075));
#49522=CARTESIAN_POINT('Ctrl Pts',(165.151916575293,-2.16951854737093,330.586115958126));
#49523=CARTESIAN_POINT('Ctrl Pts',(165.144158763771,-2.29233614551744,330.646483438239));
#49524=CARTESIAN_POINT('Ctrl Pts',(165.136400952249,-2.41276024004639,330.712043882871));
#49525=CARTESIAN_POINT('Ctrl Pts',(165.128643140727,-2.53032461331767,330.782578938055));
#49526=CARTESIAN_POINT('Ctrl Pts',(165.120891167204,-2.64780051566999,330.853060913373));
#49527=CARTESIAN_POINT('Ctrl Pts',(165.113139193681,-2.76242064645018,330.928509847599));
#49528=CARTESIAN_POINT('Ctrl Pts',(165.105387220158,-2.87374269550638,331.008661129079));
#49529=CARTESIAN_POINT('Ctrl Pts',(165.0976385296,-2.98501759960871,331.088778466444));
#49530=CARTESIAN_POINT('Ctrl Pts',(165.089889839042,-3.09299688345509,331.1735939623));
#49531=CARTESIAN_POINT('Ctrl Pts',(165.082141148485,-3.19726677859285,331.262799415471));
#49532=CARTESIAN_POINT('Ctrl Pts',(165.074394070107,-3.30151497950807,331.351986308701));
#49533=CARTESIAN_POINT('Ctrl Pts',(165.066646991729,-3.4020550299936,331.445561088553));
#49534=CARTESIAN_POINT('Ctrl Pts',(165.058899913351,-3.49850617267885,331.543175210945));
#49535=CARTESIAN_POINT('Ctrl Pts',(165.051152770045,-3.59495812371749,331.640790151437));
#49536=CARTESIAN_POINT('Ctrl Pts',(165.04340562674,-3.68732082387519,331.742444223952));
#49537=CARTESIAN_POINT('Ctrl Pts',(165.035658483434,-3.77525061624006,331.847752254806));
#49538=CARTESIAN_POINT('Ctrl Pts',(165.027909598406,-3.86320017708907,331.953083961142));
#49539=CARTESIAN_POINT('Ctrl Pts',(165.020160713378,-3.94671459652552,332.062070960508));
#49540=CARTESIAN_POINT('Ctrl Pts',(165.012411828349,-4.02549097946611,332.174295585746));
#49541=CARTESIAN_POINT('Ctrl Pts',(165.004654718575,-4.10435097647348,332.28663932736));
#49542=CARTESIAN_POINT('Ctrl Pts',(164.9968976088,-4.17846266615845,332.402227239048));
#49543=CARTESIAN_POINT('Ctrl Pts',(164.989140499025,-4.24756663703321,332.52061283248));
#49544=CARTESIAN_POINT('Ctrl Pts',(164.981379244099,-4.31670753486047,332.639061687388));
#49545=CARTESIAN_POINT('Ctrl Pts',(164.973617989173,-4.38083519912442,332.760310857596));
#49546=CARTESIAN_POINT('Ctrl Pts',(164.965856734247,-4.43973704155053,332.883890819361));
#49547=CARTESIAN_POINT('Ctrl Pts',(164.958083063842,-4.49873310772847,333.007668468791));
#49548=CARTESIAN_POINT('Ctrl Pts',(164.950309393437,-4.55248649374851,333.133784000674));
#49549=CARTESIAN_POINT('Ctrl Pts',(164.942535723033,-4.60083313928456,333.261748727324));
#49550=CARTESIAN_POINT('Ctrl Pts',(164.935123918856,-4.64692923683975,333.383756665162));
#49551=CARTESIAN_POINT('Ctrl Pts',(164.927712114678,-4.6881105425639,333.507445239027));
#49552=CARTESIAN_POINT('Ctrl Pts',(164.920300310501,-4.72427796183447,333.632381339033));
#49553=CARTESIAN_POINT('Ctrl Pts',(164.910601398758,-4.77160579175578,333.795869766224));
#49554=CARTESIAN_POINT('Ctrl Pts',(164.900902487014,-4.81047037042544,333.961910646757));
#49555=CARTESIAN_POINT('Ctrl Pts',(164.89120357527,-4.84064076570765,334.129724158747));
#49556=CARTESIAN_POINT('Ctrl Pts',(164.881648515377,-4.87036368117776,334.295048702391));
#49557=CARTESIAN_POINT('Ctrl Pts',(164.872093455484,-4.89164840743187,334.462093761431));
#49558=CARTESIAN_POINT('Ctrl Pts',(164.862538395591,-4.90431969220292,334.630092688406));
#49559=CARTESIAN_POINT('Ctrl Pts',(164.85563138923,-4.91347930454422,334.75153302162));
#49560=CARTESIAN_POINT('Ctrl Pts',(164.848724382869,-4.91813903925031,334.873471352709));
#49561=CARTESIAN_POINT('Ctrl Pts',(164.841817376508,-4.91824804142986,334.99561075504));
#49562=CARTESIAN_POINT('',(163.091817376508,-4.91461805696729,335.001889284352));
#49563=CARTESIAN_POINT('Ctrl Pts',(164.841817376508,-4.91584934655102,334.995612895733));
#49564=CARTESIAN_POINT('Ctrl Pts',(164.775232343081,-4.90575230845859,336.172498809948));
#49565=CARTESIAN_POINT('Ctrl Pts',(164.61590129823,-3.89179482935224,339.004282256428));
#49566=CARTESIAN_POINT('Ctrl Pts',(164.363824241953,0.842573010119754,340.754521664661));
#49567=CARTESIAN_POINT('Ctrl Pts',(164.08558620768,5.29506463775386,337.405564247415));
#49568=CARTESIAN_POINT('Ctrl Pts',(163.807348173406,4.88835360234718,331.849056026387));
#49569=CARTESIAN_POINT('Ctrl Pts',(163.529110139132,-0.00432738195248262,
329.184122582086));
#49570=CARTESIAN_POINT('Ctrl Pts',(163.290599873499,-4.19501065200652,331.474786607412));
#49571=CARTESIAN_POINT('Ctrl Pts',(163.144835619292,-4.90756803691727,334.062368982235));
#49572=CARTESIAN_POINT('Ctrl Pts',(163.091817376508,-4.91080196671261,335.001887817365));
#49573=CARTESIAN_POINT('',(161.341817376542,-4.91824867880592,335.003604985961));
#49574=CARTESIAN_POINT('Ctrl Pts',(163.091817376508,-4.91824963659101,335.001890680409));
#49575=CARTESIAN_POINT('Ctrl Pts',(163.08341381012,-4.91819230303736,335.151033141548));
#49576=CARTESIAN_POINT('Ctrl Pts',(163.075010243731,-4.91134684598843,335.299966218502));
#49577=CARTESIAN_POINT('Ctrl Pts',(163.066606677343,-4.8977951958724,335.4480907071));
#49578=CARTESIAN_POINT('Ctrl Pts',(163.058167104356,-4.88418548126286,335.596849861833));
#49579=CARTESIAN_POINT('Ctrl Pts',(163.049727531368,-4.86381206661228,335.744793215169));
#49580=CARTESIAN_POINT('Ctrl Pts',(163.041287958381,-4.83680856621425,335.891328197858));
#49581=CARTESIAN_POINT('Ctrl Pts',(163.032830126397,-4.80974664380272,336.038180208658));
#49582=CARTESIAN_POINT('Ctrl Pts',(163.024372294412,-4.77602603615179,336.183617493372));
#49583=CARTESIAN_POINT('Ctrl Pts',(163.015914462427,-4.7358304020831,336.327061967357));
#49584=CARTESIAN_POINT('Ctrl Pts',(163.007428609945,-4.69550160130289,336.470981667802));
#49585=CARTESIAN_POINT('Ctrl Pts',(162.998942757463,-4.64865492827412,336.612895082275));
#49586=CARTESIAN_POINT('Ctrl Pts',(162.99045690498,-4.59552346688747,336.75224060214));
#49587=CARTESIAN_POINT('Ctrl Pts',(162.984515960182,-4.55832613405275,336.849796391989));
#49588=CARTESIAN_POINT('Ctrl Pts',(162.978575015383,-4.51804937297229,336.946094016319));
#49589=CARTESIAN_POINT('Ctrl Pts',(162.972634070584,-4.47478642980206,337.040948179195));
#49590=CARTESIAN_POINT('Ctrl Pts',(162.964858991806,-4.41816701946718,337.165086445719));
#49591=CARTESIAN_POINT('Ctrl Pts',(162.957083913027,-4.3562885121357,337.287063009754));
#49592=CARTESIAN_POINT('Ctrl Pts',(162.949308834249,-4.28933803542898,337.406400274336));
#49593=CARTESIAN_POINT('Ctrl Pts',(162.9415433232,-4.22246994554613,337.525590686816));
#49594=CARTESIAN_POINT('Ctrl Pts',(162.933777812151,-4.1505424942657,337.642147924453));
#49595=CARTESIAN_POINT('Ctrl Pts',(162.926012301102,-4.0737906161863,337.755614827579));
#49596=CARTESIAN_POINT('Ctrl Pts',(162.91825448958,-3.99711483781751,337.86896922794));
#49597=CARTESIAN_POINT('Ctrl Pts',(162.910496678057,-3.91562436954204,337.9792390698));
#49598=CARTESIAN_POINT('Ctrl Pts',(162.902738866535,-3.82959957442099,338.08599257324));
#49599=CARTESIAN_POINT('Ctrl Pts',(162.894986893012,-3.7436395156861,338.192665741284));
#49600=CARTESIAN_POINT('Ctrl Pts',(162.887234919489,-3.65315216624161,338.295827534825));
#49601=CARTESIAN_POINT('Ctrl Pts',(162.879482945966,-3.55846042171278,338.395076212636));
#49602=CARTESIAN_POINT('Ctrl Pts',(162.871734255409,-3.46380877919412,338.494282858572));
#49603=CARTESIAN_POINT('Ctrl Pts',(162.863985564851,-3.36495655226675,338.589579402627));
#49604=CARTESIAN_POINT('Ctrl Pts',(162.856236874293,-3.26226588930638,338.680598365751));
#49605=CARTESIAN_POINT('Ctrl Pts',(162.848489795915,-3.15959659199617,338.771598391619));
#49606=CARTESIAN_POINT('Ctrl Pts',(162.840742717538,-3.05309073949119,338.858322347698));
#49607=CARTESIAN_POINT('Ctrl Pts',(162.83299563916,-2.94314590279378,338.940440997829));
#49608=CARTESIAN_POINT('Ctrl Pts',(162.825248495854,-2.83320014465285,339.022560336192));
#49609=CARTESIAN_POINT('Ctrl Pts',(162.817501352548,-2.71981565799548,339.100074057718));
#49610=CARTESIAN_POINT('Ctrl Pts',(162.809754209242,-2.6034211963131,339.172694709308));
#49611=CARTESIAN_POINT('Ctrl Pts',(162.802005324214,-2.48700056668453,339.245331687563));
#49612=CARTESIAN_POINT('Ctrl Pts',(162.794256439186,-2.36756894701807,339.313073200009));
#49613=CARTESIAN_POINT('Ctrl Pts',(162.786507554158,-2.24558167316801,339.37567663472));
#49614=CARTESIAN_POINT('Ctrl Pts',(162.778750444383,-2.12346492076511,339.438346517363));
#49615=CARTESIAN_POINT('Ctrl Pts',(162.770993334609,-1.99878744381306,339.495867249428));
#49616=CARTESIAN_POINT('Ctrl Pts',(162.763236224834,-1.87202714897303,339.548043251334));
#49617=CARTESIAN_POINT('Ctrl Pts',(162.755474969908,-1.74519911748454,339.600247134428));
#49618=CARTESIAN_POINT('Ctrl Pts',(162.747713714982,-1.6162864175494,339.64710046297));
#49619=CARTESIAN_POINT('Ctrl Pts',(162.739952460055,-1.48578333676146,339.688457202396));
#49620=CARTESIAN_POINT('Ctrl Pts',(162.732178789651,-1.35507149357504,339.729880099128));
#49621=CARTESIAN_POINT('Ctrl Pts',(162.724405119246,-1.22276456311469,339.765788733787));
#49622=CARTESIAN_POINT('Ctrl Pts',(162.716631448841,-1.08936914487001,339.796087773249));
#49623=CARTESIAN_POINT('Ctrl Pts',(162.709219644664,-0.962183315437024,
339.824976385134));
#49624=CARTESIAN_POINT('Ctrl Pts',(162.701807840487,-0.83400833884291,339.84876584963));
#49625=CARTESIAN_POINT('Ctrl Pts',(162.69439603631,-0.705286834752437,339.867417543547));
#49626=CARTESIAN_POINT('Ctrl Pts',(162.686620957532,-0.570256306305494,
339.886983412542));
#49627=CARTESIAN_POINT('Ctrl Pts',(162.678845878753,-0.434197600447369,
339.90095697342));
#49628=CARTESIAN_POINT('Ctrl Pts',(162.671070799975,-0.297613604147919,
339.909237130668));
#49629=CARTESIAN_POINT('Ctrl Pts',(162.663305288926,-0.161197683151326,
339.917507098655));
#49630=CARTESIAN_POINT('Ctrl Pts',(162.655539777877,-0.0242581442989326,
339.920097579706));
#49631=CARTESIAN_POINT('Ctrl Pts',(162.647774266828,0.112693440500956,339.916958740011));
#49632=CARTESIAN_POINT('Ctrl Pts',(162.640016455305,0.249509237405908,339.913823012484));
#49633=CARTESIAN_POINT('Ctrl Pts',(162.632258643783,0.386336668235516,339.904969277901));
#49634=CARTESIAN_POINT('Ctrl Pts',(162.624500832261,0.522660919506837,339.890399638651));
#49635=CARTESIAN_POINT('Ctrl Pts',(162.616748858738,0.658882582455916,339.875840963517));
#49636=CARTESIAN_POINT('Ctrl Pts',(162.608996885215,0.794601432452124,339.855574986814));
#49637=CARTESIAN_POINT('Ctrl Pts',(162.601244911692,0.929304899375981,339.829655833131));
#49638=CARTESIAN_POINT('Ctrl Pts',(162.593496221134,1.06395131930158,339.803747656225));
#49639=CARTESIAN_POINT('Ctrl Pts',(162.585747530577,1.19758282839051,339.772191137785));
#49640=CARTESIAN_POINT('Ctrl Pts',(162.577998840019,1.32969442640266,339.735091952105));
#49641=CARTESIAN_POINT('Ctrl Pts',(162.570251761641,1.46177853749345,339.698000485222));
#49642=CARTESIAN_POINT('Ctrl Pts',(162.562504683263,1.59234299043,339.655368750501));
#49643=CARTESIAN_POINT('Ctrl Pts',(162.554757604886,1.72089577501953,339.607352905305));
#49644=CARTESIAN_POINT('Ctrl Pts',(162.54701046158,1.84944963700515,339.559336657689));
#49645=CARTESIAN_POINT('Ctrl Pts',(162.539263318274,1.9759914308498,339.505936346361));
#49646=CARTESIAN_POINT('Ctrl Pts',(162.531516174968,2.10004740799503,339.447356961913));
#49647=CARTESIAN_POINT('Ctrl Pts',(162.52376728994,2.22413127555774,339.388764407575));
#49648=CARTESIAN_POINT('Ctrl Pts',(162.516018404912,2.34572786096202,339.324990630027));
#49649=CARTESIAN_POINT('Ctrl Pts',(162.508269519884,2.46438673830471,339.256287239669));
#49650=CARTESIAN_POINT('Ctrl Pts',(162.500512410109,2.58317156140579,339.187510926822));
#49651=CARTESIAN_POINT('Ctrl Pts',(162.492755300334,2.69901210892108,339.113794745235));
#49652=CARTESIAN_POINT('Ctrl Pts',(162.48499819056,2.8114852910926,339.035434737481));
#49653=CARTESIAN_POINT('Ctrl Pts',(162.477236935633,2.92401857533641,338.957032856645));
#49654=CARTESIAN_POINT('Ctrl Pts',(162.469475680707,3.03318059782353,338.873982441555));
#49655=CARTESIAN_POINT('Ctrl Pts',(162.461714425781,3.13858106759404,338.786620121512));
#49656=CARTESIAN_POINT('Ctrl Pts',(162.453940755376,3.24415014376628,338.699118050228));
#49657=CARTESIAN_POINT('Ctrl Pts',(162.446167084972,3.34594535257078,338.607290552411));
#49658=CARTESIAN_POINT('Ctrl Pts',(162.438393414567,3.44361237629537,338.511512048153));
#49659=CARTESIAN_POINT('Ctrl Pts',(162.43098161039,3.53673297656772,338.420192056313));
#49660=CARTESIAN_POINT('Ctrl Pts',(162.423569806213,3.62610087930152,338.32528082828));
#49661=CARTESIAN_POINT('Ctrl Pts',(162.416158002036,3.71144407853293,338.227129671151));
#49662=CARTESIAN_POINT('Ctrl Pts',(162.408382923258,3.80097020218334,338.124167833433));
#49663=CARTESIAN_POINT('Ctrl Pts',(162.400607844479,3.88635004042516,338.017315060586));
#49664=CARTESIAN_POINT('Ctrl Pts',(162.392832765701,3.96722643888965,337.906939532408));
#49665=CARTESIAN_POINT('Ctrl Pts',(162.385067254652,4.04800331379702,337.796699828344));
#49666=CARTESIAN_POINT('Ctrl Pts',(162.377301743603,4.12428754664072,337.682946306585));
#49667=CARTESIAN_POINT('Ctrl Pts',(162.369536232554,4.19576039019223,337.566082190927));
#49668=CARTESIAN_POINT('Ctrl Pts',(162.361778421031,4.26716236821128,337.44933394638));
#49669=CARTESIAN_POINT('Ctrl Pts',(162.354020609509,4.33376224789202,337.3294815769));
#49670=CARTESIAN_POINT('Ctrl Pts',(162.346262797987,4.39528320206433,337.206959137853));
#49671=CARTESIAN_POINT('Ctrl Pts',(162.338510824464,4.45675785976762,337.084528900826));
#49672=CARTESIAN_POINT('Ctrl Pts',(162.330758850941,4.51316102488095,336.959432941574));
#49673=CARTESIAN_POINT('Ctrl Pts',(162.323006877418,4.56426083082374,336.832131581167));
#49674=CARTESIAN_POINT('Ctrl Pts',(162.31525818686,4.61533899596838,336.704884132961));
#49675=CARTESIAN_POINT('Ctrl Pts',(162.307509496303,4.66111812372573,336.575433503225));
#49676=CARTESIAN_POINT('Ctrl Pts',(162.299760805745,4.70141379325786,336.444261543857));
#49677=CARTESIAN_POINT('Ctrl Pts',(162.292013727367,4.74170107893939,336.313116875911));
#49678=CARTESIAN_POINT('Ctrl Pts',(162.28426664899,4.77650706097572,336.180251964101));
#49679=CARTESIAN_POINT('Ctrl Pts',(162.276519570612,4.80569680047546,336.046165056002));
#49680=CARTESIAN_POINT('Ctrl Pts',(162.268772427306,4.83488678461331,335.912077024126));
#49681=CARTESIAN_POINT('Ctrl Pts',(162.261025284,4.85846034918768,335.776767357462));
#49682=CARTESIAN_POINT('Ctrl Pts',(162.253278140694,4.87633350263269,335.640745373453));
#49683=CARTESIAN_POINT('Ctrl Pts',(162.245529255666,4.89421067434204,335.504692808815));
#49684=CARTESIAN_POINT('Ctrl Pts',(162.237780370638,4.90638483382122,335.36792799563));
#49685=CARTESIAN_POINT('Ctrl Pts',(162.23003148561,4.91282381432127,335.230965867474));
#49686=CARTESIAN_POINT('Ctrl Pts',(162.222274375835,4.91926962922176,335.093858366299));
#49687=CARTESIAN_POINT('Ctrl Pts',(162.214517266061,4.91996808664918,334.956553522854));
#49688=CARTESIAN_POINT('Ctrl Pts',(162.206760156286,4.91493917697483,334.819567327964));
#49689=CARTESIAN_POINT('Ctrl Pts',(162.19899890136,4.90990758001193,334.682507932032));
#49690=CARTESIAN_POINT('Ctrl Pts',(162.191237646434,4.89914254824338,334.545767913416));
#49691=CARTESIAN_POINT('Ctrl Pts',(162.183476391507,4.88271595159642,334.409857645541));
#49692=CARTESIAN_POINT('Ctrl Pts',(162.175702721103,4.86626307774824,334.273729965531));
#49693=CARTESIAN_POINT('Ctrl Pts',(162.167929050698,4.84413060427184,334.138435074613));
#49694=CARTESIAN_POINT('Ctrl Pts',(162.160155380293,4.81644164736722,334.004473546305));
#49695=CARTESIAN_POINT('Ctrl Pts',(162.152743576116,4.79004161806783,333.876747959368));
#49696=CARTESIAN_POINT('Ctrl Pts',(162.145331771939,4.75859084167148,333.750234671884));
#49697=CARTESIAN_POINT('Ctrl Pts',(162.137919967762,4.72223754177349,333.625352531896));
#49698=CARTESIAN_POINT('Ctrl Pts',(162.130144888984,4.68410245835693,333.494349546224));
#49699=CARTESIAN_POINT('Ctrl Pts',(162.122369810205,4.64045161163237,333.364727652148));
#49700=CARTESIAN_POINT('Ctrl Pts',(162.114594731427,4.59140133512482,333.236986431614));
#49701=CARTESIAN_POINT('Ctrl Pts',(162.106829220378,4.5424114181052,333.109402404783));
#49702=CARTESIAN_POINT('Ctrl Pts',(162.099063709329,4.48803543041296,332.983694808132));
#49703=CARTESIAN_POINT('Ctrl Pts',(162.09129819828,4.42843995912629,332.86034989054));
#49704=CARTESIAN_POINT('Ctrl Pts',(162.083540386757,4.36890357692294,332.737127269792));
#49705=CARTESIAN_POINT('Ctrl Pts',(162.075782575235,4.30415817888452,332.616263015869));
#49706=CARTESIAN_POINT('Ctrl Pts',(162.068024763713,4.23441896436178,332.498224810909));
#49707=CARTESIAN_POINT('Ctrl Pts',(162.06027279019,4.16473223080954,332.380275433441));
#49708=CARTESIAN_POINT('Ctrl Pts',(162.052520816667,4.09005935892492,332.265148207032));
#49709=CARTESIAN_POINT('Ctrl Pts',(162.044768843144,4.01066196620489,332.153287219381));
#49710=CARTESIAN_POINT('Ctrl Pts',(162.037020152586,3.93129819832779,332.041473604925));
#49711=CARTESIAN_POINT('Ctrl Pts',(162.029271462029,3.84721411490942,331.932923796113));
#49712=CARTESIAN_POINT('Ctrl Pts',(162.021522771471,3.75871511479493,331.828053634074));
#49713=CARTESIAN_POINT('Ctrl Pts',(162.013775693093,3.67023452763659,331.723205291148));
#49714=CARTESIAN_POINT('Ctrl Pts',(162.006028614715,3.57734110279336,331.622035370733));
#49715=CARTESIAN_POINT('Ctrl Pts',(161.998281536338,3.48038080410419,331.524926976174));
#49716=CARTESIAN_POINT('Ctrl Pts',(161.990534393032,3.38341969279435,331.427817767753));
#49717=CARTESIAN_POINT('Ctrl Pts',(161.982787249726,3.2823919158337,331.334770429684));
#49718=CARTESIAN_POINT('Ctrl Pts',(161.97504010642,3.1776803164692,331.246131213158));
#49719=CARTESIAN_POINT('Ctrl Pts',(161.967291221392,3.07294517571416,331.157472068655));
#49720=CARTESIAN_POINT('Ctrl Pts',(161.959542336364,2.96452486280449,331.073223270247));
#49721=CARTESIAN_POINT('Ctrl Pts',(161.951793451336,2.85283498909618,330.993690527744));
#49722=CARTESIAN_POINT('Ctrl Pts',(161.944036341561,2.74102656660185,330.914073368367));
#49723=CARTESIAN_POINT('Ctrl Pts',(161.936279231786,2.62594196986935,330.839182491276));
#49724=CARTESIAN_POINT('Ctrl Pts',(161.928522122012,2.50802592453055,330.769280318388));
#49725=CARTESIAN_POINT('Ctrl Pts',(161.920760867086,2.39004686862736,330.699340792013));
#49726=CARTESIAN_POINT('Ctrl Pts',(161.912999612159,2.26923369336533,330.634395466675));
#49727=CARTESIAN_POINT('Ctrl Pts',(161.905238357233,2.14605447558744,330.574660097765));
#49728=CARTESIAN_POINT('Ctrl Pts',(161.897464686828,2.02267821120514,330.514829171733));
#49729=CARTESIAN_POINT('Ctrl Pts',(161.889691016424,1.89692869968218,330.460225012159));
#49730=CARTESIAN_POINT('Ctrl Pts',(161.881917346019,1.76929350921122,330.411014977061));
#49731=CARTESIAN_POINT('Ctrl Pts',(161.874505541842,1.64759976756455,330.364095680935));
#49732=CARTESIAN_POINT('Ctrl Pts',(161.867093737665,1.52419222532465,330.322079710591));
#49733=CARTESIAN_POINT('Ctrl Pts',(161.859681933488,1.39950331304033,330.285069084357));
#49734=CARTESIAN_POINT('Ctrl Pts',(161.85190685471,1.26870302573515,330.246244457081));
#49735=CARTESIAN_POINT('Ctrl Pts',(161.844131775931,1.13607923179781,330.212805540755));
#49736=CARTESIAN_POINT('Ctrl Pts',(161.836356697153,1.00211499508821,330.184924860491));
#49737=CARTESIAN_POINT('Ctrl Pts',(161.828591186104,0.868315609900354,330.157078489179));
#49738=CARTESIAN_POINT('Ctrl Pts',(161.820825675055,0.733179442988939,330.134776823642));
#49739=CARTESIAN_POINT('Ctrl Pts',(161.813060164006,0.597205541236013,330.118142914421));
#49740=CARTESIAN_POINT('Ctrl Pts',(161.805302352483,0.461366458002645,330.10152549777));
#49741=CARTESIAN_POINT('Ctrl Pts',(161.797544540961,0.324691678384345,330.090564701276));
#49742=CARTESIAN_POINT('Ctrl Pts',(161.789786729439,0.187690942984901,330.085332648854));
#49743=CARTESIAN_POINT('Ctrl Pts',(161.782034755916,0.0507933049835277,
330.080104533718));
#49744=CARTESIAN_POINT('Ctrl Pts',(161.774282782393,-0.0864294115402772,
330.080596596553));
#49745=CARTESIAN_POINT('Ctrl Pts',(161.76653080887,-0.223462187527487,330.08682915896));
#49746=CARTESIAN_POINT('Ctrl Pts',(161.758782118312,-0.360436930052849,
330.093059081874));
#49747=CARTESIAN_POINT('Ctrl Pts',(161.751033427755,-0.497221502372977,
330.10502465134));
#49748=CARTESIAN_POINT('Ctrl Pts',(161.743284737197,-0.633300945972124,
330.122694086452));
#49749=CARTESIAN_POINT('Ctrl Pts',(161.735537658819,-0.76935207710638,330.14035984529));
#49750=CARTESIAN_POINT('Ctrl Pts',(161.727790580441,-0.904697983955155,
330.16372705897));
#49751=CARTESIAN_POINT('Ctrl Pts',(161.720043502064,-1.03882928585775,330.19271211832));
#49752=CARTESIAN_POINT('Ctrl Pts',(161.712296358758,-1.17296171190983,330.221697420594));
#49753=CARTESIAN_POINT('Ctrl Pts',(161.704549215452,-1.30587913065618,330.256300579889));
#49754=CARTESIAN_POINT('Ctrl Pts',(161.696802072146,-1.43708319363397,330.296387031539));
#49755=CARTESIAN_POINT('Ctrl Pts',(161.689053187118,-1.5683167540705,330.336482495475));
#49756=CARTESIAN_POINT('Ctrl Pts',(161.68130430209,-1.69783581849286,330.382063590633));
#49757=CARTESIAN_POINT('Ctrl Pts',(161.673555417062,-1.82515839784708,330.432946257677));
#49758=CARTESIAN_POINT('Ctrl Pts',(161.665798307287,-1.95261611870269,330.48388293211));
#49759=CARTESIAN_POINT('Ctrl Pts',(161.658041197512,-2.07787233381947,330.540132273893));
#49760=CARTESIAN_POINT('Ctrl Pts',(161.650284087738,-2.20046570045315,330.601462315311));
#49761=CARTESIAN_POINT('Ctrl Pts',(161.642522832812,-2.32312457706218,330.662825129542));
#49762=CARTESIAN_POINT('Ctrl Pts',(161.634761577885,-2.44311742807916,330.729273863954));
#49763=CARTESIAN_POINT('Ctrl Pts',(161.627000322959,-2.56000951695535,330.800531660365));
#49764=CARTESIAN_POINT('Ctrl Pts',(161.619226652555,-2.67708859507865,330.871903446027));
#49765=CARTESIAN_POINT('Ctrl Pts',(161.61145298215,-2.7910566739831,330.948099449084));
#49766=CARTESIAN_POINT('Ctrl Pts',(161.603679311745,-2.90150916761735,331.028800230065));
#49767=CARTESIAN_POINT('Ctrl Pts',(161.596267507568,-3.00682007109914,331.105744370276));
#49768=CARTESIAN_POINT('Ctrl Pts',(161.588855703391,-3.10893509916182,331.186783152901));
#49769=CARTESIAN_POINT('Ctrl Pts',(161.581443899214,-3.20753444943506,331.271608145837));
#49770=CARTESIAN_POINT('Ctrl Pts',(161.573781304336,-3.30947007243474,331.359303333249));
#49771=CARTESIAN_POINT('Ctrl Pts',(161.566118709459,-3.40799016563838,331.451340250614));
#49772=CARTESIAN_POINT('Ctrl Pts',(161.558456114581,-3.50269411343921,331.547418790212));
#49773=CARTESIAN_POINT('Ctrl Pts',(161.550803013679,-3.59728072279349,331.643378288241));
#49774=CARTESIAN_POINT('Ctrl Pts',(161.543149912777,-3.68806030934209,331.743369166094));
#49775=CARTESIAN_POINT('Ctrl Pts',(161.535496811876,-3.77466469062467,331.847050660754));
#49776=CARTESIAN_POINT('Ctrl Pts',(161.527851236346,-3.86118391293253,331.950630204339));
#49777=CARTESIAN_POINT('Ctrl Pts',(161.520205660817,-3.9435358393365,332.057892839009));
#49778=CARTESIAN_POINT('Ctrl Pts',(161.512560085287,-4.02138896951369,332.168460874653));
#49779=CARTESIAN_POINT('Ctrl Pts',(161.504920220443,-4.09918394910211,332.278946324068));
#49780=CARTESIAN_POINT('Ctrl Pts',(161.497280355599,-4.17248658767544,332.392731933326));
#49781=CARTESIAN_POINT('Ctrl Pts',(161.489640490754,-4.24100589435396,332.509407286095));
#49782=CARTESIAN_POINT('Ctrl Pts',(161.482003627416,-4.309498281563,332.626036800126));
#49783=CARTESIAN_POINT('Ctrl Pts',(161.474366764078,-4.37321086956943,332.745553453304));
#49784=CARTESIAN_POINT('Ctrl Pts',(161.46672990074,-4.43189642539113,332.867518549411));
#49785=CARTESIAN_POINT('Ctrl Pts',(161.459094273276,-4.4905724841177,332.989463907883));
#49786=CARTESIAN_POINT('Ctrl Pts',(161.451458645813,-4.54422295440155,333.113856557851));
#49787=CARTESIAN_POINT('Ctrl Pts',(161.44382301835,-4.59264719957257,333.240234458015));
#49788=CARTESIAN_POINT('Ctrl Pts',(161.436186862408,-4.64107479629268,333.366621105072));
#49789=CARTESIAN_POINT('Ctrl Pts',(161.428550706467,-4.68427530587899,333.494992898575));
#49790=CARTESIAN_POINT('Ctrl Pts',(161.420914550525,-4.72209695484482,333.624869674705));
#49791=CARTESIAN_POINT('Ctrl Pts',(161.413272626461,-4.75994717314507,333.754844555841));
#49792=CARTESIAN_POINT('Ctrl Pts',(161.405630702397,-4.79241030582818,333.8863263019));
#49793=CARTESIAN_POINT('Ctrl Pts',(161.397988778333,-4.81938498220931,334.018821394569));
#49794=CARTESIAN_POINT('Ctrl Pts',(161.390343575079,-4.84637123356366,334.151373341568));
#49795=CARTESIAN_POINT('Ctrl Pts',(161.382698371826,-4.86786427431226,334.284939103521));
#49796=CARTESIAN_POINT('Ctrl Pts',(161.375053168573,-4.88381441428653,334.419018219471));
#49797=CARTESIAN_POINT('Ctrl Pts',(161.36739888181,-4.89978350513167,334.553256639101));
#49798=CARTESIAN_POINT('Ctrl Pts',(161.359744595046,-4.91019651712291,334.688009229207));
#49799=CARTESIAN_POINT('Ctrl Pts',(161.352090308283,-4.91505583100831,334.822773476671));
#49800=CARTESIAN_POINT('Ctrl Pts',(161.348665997702,-4.91722975007678,334.88306317481));
#49801=CARTESIAN_POINT('Ctrl Pts',(161.345241687122,-4.9182928407637,334.943355239399));
#49802=CARTESIAN_POINT('Ctrl Pts',(161.341817376542,-4.91824867880592,335.003604985961));
#49803=CARTESIAN_POINT('',(159.591817376477,-4.91824852669461,334.996193142206));
#49804=CARTESIAN_POINT('Ctrl Pts',(161.341817376508,-4.91824867880549,335.003604986558));
#49805=CARTESIAN_POINT('Ctrl Pts',(161.328946872652,-4.91808269306071,335.230057750488));
#49806=CARTESIAN_POINT('Ctrl Pts',(161.316076368796,-4.9022757372586,335.45594661472));
#49807=CARTESIAN_POINT('Ctrl Pts',(161.30320586494,-4.87106519079457,335.679637380909));
#49808=CARTESIAN_POINT('Ctrl Pts',(161.295430786162,-4.85221088173329,335.81476910136));
#49809=CARTESIAN_POINT('Ctrl Pts',(161.287655707383,-4.82769933922256,335.949329185067));
#49810=CARTESIAN_POINT('Ctrl Pts',(161.279880628605,-4.7975736730769,336.082806498826));
#49811=CARTESIAN_POINT('Ctrl Pts',(161.272115117556,-4.76748507848133,336.216119560253));
#49812=CARTESIAN_POINT('Ctrl Pts',(161.264349606507,-4.73179619149024,336.348352125223));
#49813=CARTESIAN_POINT('Ctrl Pts',(161.256584095458,-4.69060177250676,336.478999010904));
#49814=CARTESIAN_POINT('Ctrl Pts',(161.248826283936,-4.64944819790967,336.609516359819));
#49815=CARTESIAN_POINT('Ctrl Pts',(161.241068472414,-4.6028000713285,336.738450787843));
#49816=CARTESIAN_POINT('Ctrl Pts',(161.233310660892,-4.55080293398656,336.865308478113));
#49817=CARTESIAN_POINT('Ctrl Pts',(161.225558687369,-4.4988449261394,336.992070703948));
#49818=CARTESIAN_POINT('Ctrl Pts',(161.217806713846,-4.44154606734189,337.116758942513));
#49819=CARTESIAN_POINT('Ctrl Pts',(161.210054740323,-4.37910123310724,337.238896034366));
#49820=CARTESIAN_POINT('Ctrl Pts',(161.202306049765,-4.31668284429689,337.360981401088));
#49821=CARTESIAN_POINT('Ctrl Pts',(161.194557359207,-4.24912299213488,337.48051742266));
#49822=CARTESIAN_POINT('Ctrl Pts',(161.18680866865,-4.17666394771121,337.597048580676));
#49823=CARTESIAN_POINT('Ctrl Pts',(161.179061590272,-4.10421997899693,337.713555493411));
#49824=CARTESIAN_POINT('Ctrl Pts',(161.171314511894,-4.02687905178526,337.827058454403));
#49825=CARTESIAN_POINT('Ctrl Pts',(161.163567433516,-3.94492829733129,337.937128494195));
#49826=CARTESIAN_POINT('Ctrl Pts',(161.15582029021,-3.86297685605107,338.047199456481));
#49827=CARTESIAN_POINT('Ctrl Pts',(161.148073146905,-3.77641574389466,338.153837126662));
#49828=CARTESIAN_POINT('Ctrl Pts',(161.140326003599,-3.68557389822131,338.256643686873));
#49829=CARTESIAN_POINT('Ctrl Pts',(161.132577118571,-3.59471162937241,338.359473360181));
#49830=CARTESIAN_POINT('Ctrl Pts',(161.124828233543,-3.49956697070729,338.458469916748));
#49831=CARTESIAN_POINT('Ctrl Pts',(161.117079348514,-3.40050712908165,338.5532709336));
#49832=CARTESIAN_POINT('Ctrl Pts',(161.10932223874,-3.30134214431666,338.64817257323));
#49833=CARTESIAN_POINT('Ctrl Pts',(161.101565128965,-3.19825395819867,338.738869506801));
#49834=CARTESIAN_POINT('Ctrl Pts',(161.09380801919,-3.09164482727954,338.825037950721));
#49835=CARTESIAN_POINT('Ctrl Pts',(161.086046764264,-2.98497872784963,338.911252440302));
#49836=CARTESIAN_POINT('Ctrl Pts',(161.078285509338,-2.87478824845055,338.992933385753));
#49837=CARTESIAN_POINT('Ctrl Pts',(161.070524254412,-2.76150547943597,339.069799816888));
#49838=CARTESIAN_POINT('Ctrl Pts',(161.062750584007,-2.64804149490968,339.146789209263));
#49839=CARTESIAN_POINT('Ctrl Pts',(161.054976913602,-2.5314756684073,339.218948491291));
#49840=CARTESIAN_POINT('Ctrl Pts',(161.047203243198,-2.41226635401111,339.286041775322));
#49841=CARTESIAN_POINT('Ctrl Pts',(161.039791439021,-2.29860626187827,339.350011850841));
#49842=CARTESIAN_POINT('Ctrl Pts',(161.032379634843,-2.18254350827548,339.409376827658));
#49843=CARTESIAN_POINT('Ctrl Pts',(161.024967830666,-2.06449130336647,339.463973422952));
#49844=CARTESIAN_POINT('Ctrl Pts',(161.017192751888,-1.94065300823737,339.521245960016));
#49845=CARTESIAN_POINT('Ctrl Pts',(161.009417673109,-1.81423396101038,339.573451863338));
#49846=CARTESIAN_POINT('Ctrl Pts',(161.001642594331,-1.68568731369463,339.620350781375));
#49847=CARTESIAN_POINT('Ctrl Pts',(160.993877083282,-1.55729885121218,339.667191987307));
#49848=CARTESIAN_POINT('Ctrl Pts',(160.986111572233,-1.42678836169221,339.708739069256));
#49849=CARTESIAN_POINT('Ctrl Pts',(160.978346061184,-1.29463194444584,339.744798329847));
#49850=CARTESIAN_POINT('Ctrl Pts',(160.970588249662,-1.16260656067179,339.780821837577));
#49851=CARTESIAN_POINT('Ctrl Pts',(160.962830438139,-1.02893887148868,339.81136825));
#49852=CARTESIAN_POINT('Ctrl Pts',(160.955072626617,-0.89412289873917,339.836292723197));
#49853=CARTESIAN_POINT('Ctrl Pts',(160.947320653094,-0.759408379284553,
339.861198439937));
#49854=CARTESIAN_POINT('Ctrl Pts',(160.939568679571,-0.623547679064922,
339.880490567654));
#49855=CARTESIAN_POINT('Ctrl Pts',(160.931816706048,-0.48704750995685,339.89407476297));
#49856=CARTESIAN_POINT('Ctrl Pts',(160.92406801549,-0.350605148751389,339.907653205372));
#49857=CARTESIAN_POINT('Ctrl Pts',(160.916319324933,-0.213524245433846,
339.915528484611));
#49858=CARTESIAN_POINT('Ctrl Pts',(160.908570634375,-0.076318961938044,
339.917657824468));
#49859=CARTESIAN_POINT('Ctrl Pts',(160.900823555997,0.0608577748525656,
339.919786721298));
#49860=CARTESIAN_POINT('Ctrl Pts',(160.89307647762,0.198158449765743,339.9161720506));
#49861=CARTESIAN_POINT('Ctrl Pts',(160.885329399242,0.335066950037492,339.906823127186));
#49862=CARTESIAN_POINT('Ctrl Pts',(160.877582255936,0.471976597734317,339.89747412542));
#49863=CARTESIAN_POINT('Ctrl Pts',(160.86983511263,0.608493674267794,339.88239080171));
#49864=CARTESIAN_POINT('Ctrl Pts',(160.862087969324,0.744105639228933,339.861634484427));
#49865=CARTESIAN_POINT('Ctrl Pts',(160.854339084296,0.879748092638826,339.840873500683));
#49866=CARTESIAN_POINT('Ctrl Pts',(160.846590199268,1.0144846432581,339.814437044568));
#49867=CARTESIAN_POINT('Ctrl Pts',(160.83884131424,1.14781180517559,339.782437780296));
#49868=CARTESIAN_POINT('Ctrl Pts',(160.831084204465,1.28128048192034,339.750404551673));
#49869=CARTESIAN_POINT('Ctrl Pts',(160.823327094691,1.41333640100232,339.712796811621));
#49870=CARTESIAN_POINT('Ctrl Pts',(160.815569984916,1.54348960178851,339.669777608374));
#49871=CARTESIAN_POINT('Ctrl Pts',(160.80780872999,1.67371235228364,339.62673541704));
#49872=CARTESIAN_POINT('Ctrl Pts',(160.800047475063,1.80202999303155,339.578276138538));
#49873=CARTESIAN_POINT('Ctrl Pts',(160.792286220137,1.92797242132446,339.524611077774));
#49874=CARTESIAN_POINT('Ctrl Pts',(160.784512549733,2.0541163164581,339.470860170402));
#49875=CARTESIAN_POINT('Ctrl Pts',(160.776738879328,2.17787705343211,339.411887008077));
#49876=CARTESIAN_POINT('Ctrl Pts',(160.768965208923,2.29880822759548,339.347949378183));
#49877=CARTESIAN_POINT('Ctrl Pts',(160.761553404746,2.41411002650719,339.286988060343));
#49878=CARTESIAN_POINT('Ctrl Pts',(160.754141600569,2.52683951766054,339.221514210066));
#49879=CARTESIAN_POINT('Ctrl Pts',(160.746729796392,2.6366357813195,339.151786942892));
#49880=CARTESIAN_POINT('Ctrl Pts',(160.738954717614,2.75181348692667,339.078642134646));
#49881=CARTESIAN_POINT('Ctrl Pts',(160.731179638835,2.86412714517176,339.000585270662));
#49882=CARTESIAN_POINT('Ctrl Pts',(160.723404560057,2.97312941276129,338.917867348121));
#49883=CARTESIAN_POINT('Ctrl Pts',(160.715639049008,3.08199754612111,338.83525121525));
#49884=CARTESIAN_POINT('Ctrl Pts',(160.707873537959,3.18756208826918,338.747985670306));
#49885=CARTESIAN_POINT('Ctrl Pts',(160.70010802691,3.28940251029697,338.656366254596));
#49886=CARTESIAN_POINT('Ctrl Pts',(160.692350215388,3.39114195724982,338.564837679804));
#49887=CARTESIAN_POINT('Ctrl Pts',(160.684592403866,3.48916434360316,338.46896408481));
#49888=CARTESIAN_POINT('Ctrl Pts',(160.676834592343,3.58308052344825,338.369082519765));
#49889=CARTESIAN_POINT('Ctrl Pts',(160.66908261882,3.67692602838971,338.269276118765));
#49890=CARTESIAN_POINT('Ctrl Pts',(160.661330645297,3.76667121074038,338.165468034779));
#49891=CARTESIAN_POINT('Ctrl Pts',(160.653578671774,3.85196252427038,338.058033318019));
#49892=CARTESIAN_POINT('Ctrl Pts',(160.645829981217,3.9372177168785,337.950644099926));
#49893=CARTESIAN_POINT('Ctrl Pts',(160.638081290659,4.01802254968772,337.839631609313));
#49894=CARTESIAN_POINT('Ctrl Pts',(160.630332600102,4.09406280873805,337.725405067253));
#49895=CARTESIAN_POINT('Ctrl Pts',(160.622585521724,4.17008724697739,337.611202290979));
#49896=CARTESIAN_POINT('Ctrl Pts',(160.614838443346,4.24134886677871,337.493787118539));
#49897=CARTESIAN_POINT('Ctrl Pts',(160.607091364968,4.3075762029348,337.373598600945));
#49898=CARTESIAN_POINT('Ctrl Pts',(160.599344221662,4.37380409413971,337.253409076056));
#49899=CARTESIAN_POINT('Ctrl Pts',(160.591597078357,4.434997428904,337.130446501995));
#49900=CARTESIAN_POINT('Ctrl Pts',(160.583849935051,4.49093041453717,337.005175073226));
#49901=CARTESIAN_POINT('Ctrl Pts',(160.576101050023,4.54687597509297,336.879875480779));
#49902=CARTESIAN_POINT('Ctrl Pts',(160.568352164995,4.59755867387115,336.752266357558));
#49903=CARTESIAN_POINT('Ctrl Pts',(160.560603279966,4.64280078749434,336.622832064676));
#49904=CARTESIAN_POINT('Ctrl Pts',(160.552846170192,4.68809092156441,336.493260388898));
#49905=CARTESIAN_POINT('Ctrl Pts',(160.545089060417,4.72792880581079,336.361860043179));
#49906=CARTESIAN_POINT('Ctrl Pts',(160.537331950642,4.76218640516041,336.229131280623));
#49907=CARTESIAN_POINT('Ctrl Pts',(160.529570695716,4.79646231067577,336.09633159206));
#49908=CARTESIAN_POINT('Ctrl Pts',(160.52180944079,4.82515190782318,335.962202454228));
#49909=CARTESIAN_POINT('Ctrl Pts',(160.514048185864,4.84817848785695,335.827253535732));
#49910=CARTESIAN_POINT('Ctrl Pts',(160.506274515459,4.87124190291443,335.692088742947));
#49911=CARTESIAN_POINT('Ctrl Pts',(160.498500845055,4.88862414874428,335.556101936892));
#49912=CARTESIAN_POINT('Ctrl Pts',(160.49072717465,4.9003004290861,335.419808012309));
#49913=CARTESIAN_POINT('Ctrl Pts',(160.483315370473,4.91143317576882,335.289858602705));
#49914=CARTESIAN_POINT('Ctrl Pts',(160.475903566296,4.91737921432763,335.159630311343));
#49915=CARTESIAN_POINT('Ctrl Pts',(160.468491762119,4.91816112616878,335.029566865614));
#49916=CARTESIAN_POINT('Ctrl Pts',(160.46071668334,4.91898136183845,334.893128622971));
#49917=CARTESIAN_POINT('Ctrl Pts',(160.452941604562,4.91412104467701,334.756440623642));
#49918=CARTESIAN_POINT('Ctrl Pts',(160.445166525784,4.90354916044425,334.620014877125));
#49919=CARTESIAN_POINT('Ctrl Pts',(160.437401014735,4.89299028558807,334.483757011173));
#49920=CARTESIAN_POINT('Ctrl Pts',(160.429635503686,4.87673385816498,334.347761141896));
#49921=CARTESIAN_POINT('Ctrl Pts',(160.421869992637,4.85480083284138,334.212540835381));
#49922=CARTESIAN_POINT('Ctrl Pts',(160.414112181114,4.83288955417625,334.077454600194));
#49923=CARTESIAN_POINT('Ctrl Pts',(160.406354369592,4.80531294055152,333.943142780816));
#49924=CARTESIAN_POINT('Ctrl Pts',(160.39859655807,4.77214383544901,333.810115015522));
#49925=CARTESIAN_POINT('Ctrl Pts',(160.390844584547,4.73899969114995,333.67718735784));
#49926=CARTESIAN_POINT('Ctrl Pts',(160.383092611024,4.70027152642522,333.54554220862));
#49927=CARTESIAN_POINT('Ctrl Pts',(160.375340637501,4.65608340484845,333.415679833621));
#49928=CARTESIAN_POINT('Ctrl Pts',(160.367591946943,4.61191399696739,333.285872455415));
#49929=CARTESIAN_POINT('Ctrl Pts',(160.359843256386,4.56228935687671,333.157846719044));
#49930=CARTESIAN_POINT('Ctrl Pts',(160.352094565828,4.50738356810354,333.032088306735));
#49931=CARTESIAN_POINT('Ctrl Pts',(160.34434748745,4.4524892029383,332.906356059513));
#49932=CARTESIAN_POINT('Ctrl Pts',(160.336600409073,4.39231603095595,332.782890556034));
#49933=CARTESIAN_POINT('Ctrl Pts',(160.328853330695,4.32708635411989,332.662157672877));
#49934=CARTESIAN_POINT('Ctrl Pts',(160.321106187389,4.26185613059634,332.541423777861));
#49935=CARTESIAN_POINT('Ctrl Pts',(160.313359044083,4.19156950349053,332.42342289274));
#49936=CARTESIAN_POINT('Ctrl Pts',(160.305611900777,4.11649463444983,332.308596093663));
#49937=CARTESIAN_POINT('Ctrl Pts',(160.297863015749,4.04140288698472,332.193743479084));
#49938=CARTESIAN_POINT('Ctrl Pts',(160.290114130721,3.96152096932861,332.082066697628));
#49939=CARTESIAN_POINT('Ctrl Pts',(160.282365245693,3.87716001475814,331.973977316268));
#49940=CARTESIAN_POINT('Ctrl Pts',(160.274608135918,3.79270951859882,331.865773207721));
#49941=CARTESIAN_POINT('Ctrl Pts',(160.266851026144,3.70377072964302,331.761164414135));
#49942=CARTESIAN_POINT('Ctrl Pts',(160.259093916369,3.6106950342744,331.660529318595));
#49943=CARTESIAN_POINT('Ctrl Pts',(160.251332661443,3.51756960223016,331.559840446876));
#49944=CARTESIAN_POINT('Ctrl Pts',(160.243571406517,3.42030313593273,331.46312977976));
#49945=CARTESIAN_POINT('Ctrl Pts',(160.23581015159,3.31928271508222,331.370737634194));
#49946=CARTESIAN_POINT('Ctrl Pts',(160.228036481186,3.21810069448084,331.278197691305));
#49947=CARTESIAN_POINT('Ctrl Pts',(160.220262810781,3.11315301873013,331.189990326276));
#49948=CARTESIAN_POINT('Ctrl Pts',(160.212489140376,3.00485925512245,331.106415029898));
#49949=CARTESIAN_POINT('Ctrl Pts',(160.205077336199,2.90160659226398,331.026730183673));
#49950=CARTESIAN_POINT('Ctrl Pts',(160.197665532022,2.7953125864056,330.951256032041));
#49951=CARTESIAN_POINT('Ctrl Pts',(160.190253727845,2.68636259747263,330.880213712169));
#49952=CARTESIAN_POINT('Ctrl Pts',(160.182478649067,2.57207264503745,330.805689396576));
#49953=CARTESIAN_POINT('Ctrl Pts',(160.174703570288,2.45449859379039,330.735806821375));
#49954=CARTESIAN_POINT('Ctrl Pts',(160.16692849151,2.33405421985501,330.670869144819));
#49955=CARTESIAN_POINT('Ctrl Pts',(160.159162980461,2.21375806038963,330.606011378209));
#49956=CARTESIAN_POINT('Ctrl Pts',(160.151397469412,2.09059894689708,330.546086586537));
#49957=CARTESIAN_POINT('Ctrl Pts',(160.143631958363,1.96502008783066,330.491355068657));
#49958=CARTESIAN_POINT('Ctrl Pts',(160.13587414684,1.83956574056873,330.436677817237));
#49959=CARTESIAN_POINT('Ctrl Pts',(160.128116335318,1.71169677825932,330.38718374768));
#49960=CARTESIAN_POINT('Ctrl Pts',(160.120358523796,1.58188118638672,330.34308739886));
#49961=CARTESIAN_POINT('Ctrl Pts',(160.112606550273,1.45216328486356,330.299024233941));
#49962=CARTESIAN_POINT('Ctrl Pts',(160.10485457675,1.32050203820445,330.260350829848));
#49963=CARTESIAN_POINT('Ctrl Pts',(160.097102603227,1.18738526847622,330.22723358138));
#49964=CARTESIAN_POINT('Ctrl Pts',(160.089353912669,1.05432487377899,330.194130358087));
#49965=CARTESIAN_POINT('Ctrl Pts',(160.081605222112,0.919810560541087,330.166578704569));
#49966=CARTESIAN_POINT('Ctrl Pts',(160.073856531554,0.784344955893373,330.144695060795));
#49967=CARTESIAN_POINT('Ctrl Pts',(160.066109453176,0.648907535996137,330.122815970097));
#49968=CARTESIAN_POINT('Ctrl Pts',(160.058362374799,0.51251960400369,330.106602605773));
#49969=CARTESIAN_POINT('Ctrl Pts',(160.050615296421,0.375693225819414,330.096120141911));
#49970=CARTESIAN_POINT('Ctrl Pts',(160.042868153115,0.238865700898394,330.085637590195));
#49971=CARTESIAN_POINT('Ctrl Pts',(160.035121009809,0.101600112188512,330.0808860646));
#49972=CARTESIAN_POINT('Ctrl Pts',(160.027373866503,-0.0355875123107284,
330.081878753887));
#49973=CARTESIAN_POINT('Ctrl Pts',(160.019624981475,-0.172805979500602,
330.082871666352));
#49974=CARTESIAN_POINT('Ctrl Pts',(160.011876096447,-0.309946056813376,
330.089611360657));
#49975=CARTESIAN_POINT('Ctrl Pts',(160.004127211419,-0.446493276734069,
330.102058920696));
#49976=CARTESIAN_POINT('Ctrl Pts',(159.996370101644,-0.583185429284782,
330.114519692704));
#49977=CARTESIAN_POINT('Ctrl Pts',(159.98861299187,-0.719283077552539,330.132700397102));
#49978=CARTESIAN_POINT('Ctrl Pts',(159.980855882095,-0.854277875794783,
330.156510310383));
#49979=CARTESIAN_POINT('Ctrl Pts',(159.973094627169,-0.989344810940912,
330.18033294692));
#49980=CARTESIAN_POINT('Ctrl Pts',(159.965333372242,-1.12330734021289,330.209790702285));
#49981=CARTESIAN_POINT('Ctrl Pts',(159.957572117316,-1.25566981279231,330.244742237928));
#49982=CARTESIAN_POINT('Ctrl Pts',(159.949798446912,-1.38824402219101,330.279749684638));
#49983=CARTESIAN_POINT('Ctrl Pts',(159.942024776507,-1.51921268651118,330.320268357582));
#49984=CARTESIAN_POINT('Ctrl Pts',(159.934251106102,-1.64809690561911,330.366107505327));
#49985=CARTESIAN_POINT('Ctrl Pts',(159.926839301925,-1.77098153331938,330.409812829715));
#49986=CARTESIAN_POINT('Ctrl Pts',(159.919427497748,-1.89197114331462,330.45835433277));
#49987=CARTESIAN_POINT('Ctrl Pts',(159.912015693571,-2.01067123627604,330.511527627119));
#49988=CARTESIAN_POINT('Ctrl Pts',(159.904240614793,-2.13518917438329,330.56730710302));
#49989=CARTESIAN_POINT('Ctrl Pts',(159.896465536014,-2.25758098827673,330.628360159743));
#49990=CARTESIAN_POINT('Ctrl Pts',(159.888690457236,-2.37736782771031,330.694502900446));
#49991=CARTESIAN_POINT('Ctrl Pts',(159.880924946187,-2.497007261812,330.760564248296));
#49992=CARTESIAN_POINT('Ctrl Pts',(159.873159435138,-2.61404776074752,330.831702631058));
#49993=CARTESIAN_POINT('Ctrl Pts',(159.865393924089,-2.72803058813252,330.907686207936));
#49994=CARTESIAN_POINT('Ctrl Pts',(159.857636112566,-2.84190040121241,330.983594446877));
#49995=CARTESIAN_POINT('Ctrl Pts',(159.849878301044,-2.95271825283825,331.064338104241));
#49996=CARTESIAN_POINT('Ctrl Pts',(159.842120489522,-3.06005047889474,331.149639740347));
#49997=CARTESIAN_POINT('Ctrl Pts',(159.834368515999,-3.16730193404739,331.234877184266));
#49998=CARTESIAN_POINT('Ctrl Pts',(159.826616542476,-3.27107267989869,331.324665537417));
#49999=CARTESIAN_POINT('Ctrl Pts',(159.818864568953,-3.37095880299916,331.41868462559));
#50000=CARTESIAN_POINT('Ctrl Pts',(159.811115878395,-3.4708026242671,331.512663896624));
#50001=CARTESIAN_POINT('Ctrl Pts',(159.803367187838,-3.56676481082179,331.610870071731));
#50002=CARTESIAN_POINT('Ctrl Pts',(159.79561849728,-3.65847544542785,331.712943493382));
#50003=CARTESIAN_POINT('Ctrl Pts',(159.787871418902,-3.7501669988704,331.814995677805));
#50004=CARTESIAN_POINT('Ctrl Pts',(159.780124340524,-3.837608498766,331.920913217768));
#50005=CARTESIAN_POINT('Ctrl Pts',(159.772377262147,-3.92046803059277,332.030300775567));
#50006=CARTESIAN_POINT('Ctrl Pts',(159.764630118841,-4.00332825686225,332.139689250138));
#50007=CARTESIAN_POINT('Ctrl Pts',(159.756882975535,-4.08160620245395,332.252547488975));
#50008=CARTESIAN_POINT('Ctrl Pts',(159.749135832229,-4.15501152429481,332.36844869032));
#50009=CARTESIAN_POINT('Ctrl Pts',(159.741386947201,-4.22843334921032,332.484375948716));
#50010=CARTESIAN_POINT('Ctrl Pts',(159.733638062173,-4.29698016141381,332.603347200795));
#50011=CARTESIAN_POINT('Ctrl Pts',(159.725889177145,-4.36040627839692,332.724908760112));
#50012=CARTESIAN_POINT('Ctrl Pts',(159.71813206737,-4.423899716516,332.846599346123));
#50013=CARTESIAN_POINT('Ctrl Pts',(159.710374957595,-4.48226142107828,332.970885384426));
#50014=CARTESIAN_POINT('Ctrl Pts',(159.702617847821,-4.53529258836708,333.097290300544));
#50015=CARTESIAN_POINT('Ctrl Pts',(159.694856592894,-4.58835209381604,333.223762763408));
#50016=CARTESIAN_POINT('Ctrl Pts',(159.687095337968,-4.63607525023321,333.352355993952));
#50017=CARTESIAN_POINT('Ctrl Pts',(159.679334083042,-4.67831268712215,333.482576702429));
#50018=CARTESIAN_POINT('Ctrl Pts',(159.671560412637,-4.72061769014494,333.6130057216));
#50019=CARTESIAN_POINT('Ctrl Pts',(159.663786742233,-4.75741933288212,333.745067044412));
#50020=CARTESIAN_POINT('Ctrl Pts',(159.656013071828,-4.78861886194275,333.878254726978));
#50021=CARTESIAN_POINT('Ctrl Pts',(159.648601267651,-4.81836604541947,334.005242490878));
#50022=CARTESIAN_POINT('Ctrl Pts',(159.641189463474,-4.84302088026373,334.133253827738));
#50023=CARTESIAN_POINT('Ctrl Pts',(159.633777659297,-4.86254175395446,334.261846388921));
#50024=CARTESIAN_POINT('Ctrl Pts',(159.620632863804,-4.89716192016204,334.489904615808));
#50025=CARTESIAN_POINT('Ctrl Pts',(159.607488068311,-4.91574372033797,334.72045707603));
#50026=CARTESIAN_POINT('Ctrl Pts',(159.594343272817,-4.91801323229811,334.95174122421));
#50027=CARTESIAN_POINT('Ctrl Pts',(159.593501307381,-4.91815860166723,334.966555700317));
#50028=CARTESIAN_POINT('Ctrl Pts',(159.592659341944,-4.91823705562696,334.981373162964));
#50029=CARTESIAN_POINT('Ctrl Pts',(159.591817376508,-4.91824852669419,334.996193141659));
#50030=CARTESIAN_POINT('',(157.841817376542,-4.91824974369148,334.99841217802));
#50031=CARTESIAN_POINT('Ctrl Pts',(159.591817376477,-4.91824852669461,334.996193142206));
#50032=CARTESIAN_POINT('Ctrl Pts',(159.584166148112,-4.91835276819738,335.130867365703));
#50033=CARTESIAN_POINT('Ctrl Pts',(159.576514919747,-4.91292126616045,335.265748454898));
#50034=CARTESIAN_POINT('Ctrl Pts',(159.568863691381,-4.90192965851686,335.400335715934));
#50035=CARTESIAN_POINT('Ctrl Pts',(159.561220060556,-4.89094896535318,335.534789334105));
#50036=CARTESIAN_POINT('Ctrl Pts',(159.553576429731,-4.87441917997282,335.668949305156));
#50037=CARTESIAN_POINT('Ctrl Pts',(159.545932798906,-4.85236797623589,335.802314206343));
#50038=CARTESIAN_POINT('Ctrl Pts',(159.537999749994,-4.82948182673326,335.940728830026));
#50039=CARTESIAN_POINT('Ctrl Pts',(159.530066701082,-4.80064787934645,336.078286547999));
#50040=CARTESIAN_POINT('Ctrl Pts',(159.52213365217,-4.76595634042732,336.214431234628));
#50041=CARTESIAN_POINT('Ctrl Pts',(159.514498681209,-4.7325683082593,336.34546039385));
#50042=CARTESIAN_POINT('Ctrl Pts',(159.506863710247,-4.69375501710053,336.47518035946));
#50043=CARTESIAN_POINT('Ctrl Pts',(159.499228739286,-4.64964898909618,336.603105530119));
#50044=CARTESIAN_POINT('Ctrl Pts',(159.491594952606,-4.60554980250131,336.731010857945));
#50045=CARTESIAN_POINT('Ctrl Pts',(159.483961165926,-4.55615964273177,336.857121563007));
#50046=CARTESIAN_POINT('Ctrl Pts',(159.476327379246,-4.50166060189852,336.980968169309));
#50047=CARTESIAN_POINT('Ctrl Pts',(159.468693011005,-4.44715740918385,337.104824210573));
#50048=CARTESIAN_POINT('Ctrl Pts',(159.461058642763,-4.38754472437907,337.226415440962));
#50049=CARTESIAN_POINT('Ctrl Pts',(159.453424274521,-4.32305215521528,337.345293825044));
#50050=CARTESIAN_POINT('Ctrl Pts',(159.445787558591,-4.25853975357349,337.464208766096));
#50051=CARTESIAN_POINT('Ctrl Pts',(159.438150842661,-4.18914467634525,337.58040884784));
#50052=CARTESIAN_POINT('Ctrl Pts',(159.430514126731,-4.11514140890666,337.693472525793));
#50053=CARTESIAN_POINT('Ctrl Pts',(159.422869241791,-4.04105898002964,337.806657148181));
#50054=CARTESIAN_POINT('Ctrl Pts',(159.415224356851,-3.96235874420188,337.916698333462));
#50055=CARTESIAN_POINT('Ctrl Pts',(159.407579471911,-3.87935739097104,338.023205136212));
#50056=CARTESIAN_POINT('Ctrl Pts',(159.399929727442,-3.79630327729702,338.129779640824));
#50057=CARTESIAN_POINT('Ctrl Pts',(159.392279982972,-3.70894286462007,338.232814984739));
#50058=CARTESIAN_POINT('Ctrl Pts',(159.384630238503,-3.61763077036886,338.33195598287));
#50059=CARTESIAN_POINT('Ctrl Pts',(159.376969842564,-3.52619153357005,338.431235024478));
#50060=CARTESIAN_POINT('Ctrl Pts',(159.369309446625,-3.43078992058651,338.526608617573));
#50061=CARTESIAN_POINT('Ctrl Pts',(159.361649050686,-3.33181489974728,338.617760707443));
#50062=CARTESIAN_POINT('Ctrl Pts',(159.359612575465,-3.3055029206965,338.641993002206));
#50063=CARTESIAN_POINT('Ctrl Pts',(159.357576100244,-3.27893856162204,338.665927182308));
#50064=CARTESIAN_POINT('Ctrl Pts',(159.355539625023,-3.25212947502574,338.689557824478));
#50065=CARTESIAN_POINT('Ctrl Pts',(159.347764546244,-3.14977479961162,338.779777485656));
#50066=CARTESIAN_POINT('Ctrl Pts',(159.339989467466,-3.04350126674975,338.865877242081));
#50067=CARTESIAN_POINT('Ctrl Pts',(159.332214388687,-2.93367463500481,338.947497460218));
#50068=CARTESIAN_POINT('Ctrl Pts',(159.324448877638,-2.82398315192221,339.029017239481));
#50069=CARTESIAN_POINT('Ctrl Pts',(159.316683366589,-2.71074758033384,339.106068217542));
#50070=CARTESIAN_POINT('Ctrl Pts',(159.30891785554,-2.59436898147057,339.178328930384));
#50071=CARTESIAN_POINT('Ctrl Pts',(159.301160044018,-2.47810577232699,339.250517996519));
#50072=CARTESIAN_POINT('Ctrl Pts',(159.293402232496,-2.35870606749338,339.317926044473));
#50073=CARTESIAN_POINT('Ctrl Pts',(159.285644420974,-2.23660204226525,339.380273321042));
#50074=CARTESIAN_POINT('Ctrl Pts',(159.277892447451,-2.11458990418783,339.442573679309));
#50075=CARTESIAN_POINT('Ctrl Pts',(159.270140473928,-1.98987784317406,339.499820669568));
#50076=CARTESIAN_POINT('Ctrl Pts',(159.262388500405,-1.86292460336547,339.551779320736));
#50077=CARTESIAN_POINT('Ctrl Pts',(159.254639809847,-1.73602512832963,339.603715967383));
#50078=CARTESIAN_POINT('Ctrl Pts',(159.246891119289,-1.6068867232691,339.650368581628));
#50079=CARTESIAN_POINT('Ctrl Pts',(159.239142428732,-1.47598998319402,339.691549491587));
#50080=CARTESIAN_POINT('Ctrl Pts',(159.231395350354,-1.34512047727888,339.732721833514));
#50081=CARTESIAN_POINT('Ctrl Pts',(159.223648271976,-1.21249373664676,339.768424618352));
#50082=CARTESIAN_POINT('Ctrl Pts',(159.215901193598,-1.07860708589481,339.798519544272));
#50083=CARTESIAN_POINT('Ctrl Pts',(159.208154050293,-0.944719313043811,
339.828614722416));
#50084=CARTESIAN_POINT('Ctrl Pts',(159.200406906987,-0.809571990370545,
339.853101862176));
#50085=CARTESIAN_POINT('Ctrl Pts',(159.192659763681,-0.673673856271418,
339.871893533102));
#50086=CARTESIAN_POINT('Ctrl Pts',(159.184910878653,-0.537745169386592,
339.890689428794));
#50087=CARTESIAN_POINT('Ctrl Pts',(159.177161993625,-0.401065722300536,
339.903787254145));
#50088=CARTESIAN_POINT('Ctrl Pts',(159.169413108597,-0.264150219528999,
339.911151364397));
#50089=CARTESIAN_POINT('Ctrl Pts',(159.161655998822,-0.127089393228288,
339.918523290993));
#50090=CARTESIAN_POINT('Ctrl Pts',(159.153898889047,0.0102075983322991,
339.920149324457));
#50091=CARTESIAN_POINT('Ctrl Pts',(159.146141779273,0.147224641051112,339.916045968822));
#50092=CARTESIAN_POINT('Ctrl Pts',(159.138380524346,0.284314901296692,339.911940420484));
#50093=CARTESIAN_POINT('Ctrl Pts',(159.13061926942,0.421124524948384,339.902099410557));
#50094=CARTESIAN_POINT('Ctrl Pts',(159.122858014494,0.557142664695376,339.886591359391));
#50095=CARTESIAN_POINT('Ctrl Pts',(159.115084344089,0.693378389137686,339.871058500398));
#50096=CARTESIAN_POINT('Ctrl Pts',(159.107310673685,0.828819713232416,339.849840545302));
#50097=CARTESIAN_POINT('Ctrl Pts',(159.09953700328,0.962965243144901,339.823057225764));
#50098=CARTESIAN_POINT('Ctrl Pts',(159.092125199103,1.09086626636593,339.797520676194));
#50099=CARTESIAN_POINT('Ctrl Pts',(159.084713394926,1.21758913919218,339.76692530484));
#50100=CARTESIAN_POINT('Ctrl Pts',(159.077301590749,1.34271402178142,339.731416502297));
#50101=CARTESIAN_POINT('Ctrl Pts',(159.06952651197,1.47397164759447,339.694167307567));
#50102=CARTESIAN_POINT('Ctrl Pts',(159.061751433192,1.60388547623542,339.651393145142));
#50103=CARTESIAN_POINT('Ctrl Pts',(159.053976354414,1.73195515124559,339.60320697086));
#50104=CARTESIAN_POINT('Ctrl Pts',(159.046210843365,1.85986722836722,339.555080092734));
#50105=CARTESIAN_POINT('Ctrl Pts',(159.038445332316,1.98593930487157,339.501554590223));
#50106=CARTESIAN_POINT('Ctrl Pts',(159.030679821267,2.10968401756242,339.442793761648));
#50107=CARTESIAN_POINT('Ctrl Pts',(159.022922009744,2.23330603701076,339.384091194606));
#50108=CARTESIAN_POINT('Ctrl Pts',(159.015164198222,2.35460493406293,339.320163798152));
#50109=CARTESIAN_POINT('Ctrl Pts',(159.0074063867,2.47311158342917,339.251223607199));
#50110=CARTESIAN_POINT('Ctrl Pts',(158.999654413177,2.59152905278352,339.182335295927));
#50111=CARTESIAN_POINT('Ctrl Pts',(158.991902439654,2.70715812039472,339.108441894467));
#50112=CARTESIAN_POINT('Ctrl Pts',(158.984150466131,2.81955294128599,339.029802014217));
#50113=CARTESIAN_POINT('Ctrl Pts',(158.976401775573,2.9319001629039,338.951195438003));
#50114=CARTESIAN_POINT('Ctrl Pts',(158.968653085016,3.04101554245042,338.867846604634));
#50115=CARTESIAN_POINT('Ctrl Pts',(158.960904394458,3.14648118509957,338.780058096685));
#50116=CARTESIAN_POINT('Ctrl Pts',(158.95315731608,3.25192488474078,338.692287853868));
#50117=CARTESIAN_POINT('Ctrl Pts',(158.945410237703,3.35372005767317,338.600080023705));
#50118=CARTESIAN_POINT('Ctrl Pts',(158.937663159325,3.45148127206204,338.503777974003));
#50119=CARTESIAN_POINT('Ctrl Pts',(158.929916016019,3.54924330578419,338.407475117196));
#50120=CARTESIAN_POINT('Ctrl Pts',(158.922168872713,3.64297103506913,338.307078246715));
#50121=CARTESIAN_POINT('Ctrl Pts',(158.914421729407,3.73231563024755,338.202967857895));
#50122=CARTESIAN_POINT('Ctrl Pts',(158.906672844379,3.82168031198779,338.09883406285));
#50123=CARTESIAN_POINT('Ctrl Pts',(158.898923959351,3.90665964423886,337.990985384718));
#50124=CARTESIAN_POINT('Ctrl Pts',(158.891175074323,3.98694511641619,337.879835360083));
#50125=CARTESIAN_POINT('Ctrl Pts',(158.883417964548,4.06731580442318,337.768567359664));
#50126=CARTESIAN_POINT('Ctrl Pts',(158.875660854774,4.14298245088689,337.653991330368));
#50127=CARTESIAN_POINT('Ctrl Pts',(158.867903744999,4.21367963544295,337.53655021483));
#50128=CARTESIAN_POINT('Ctrl Pts',(158.860142490073,4.28441459831389,337.419046342515));
#50129=CARTESIAN_POINT('Ctrl Pts',(158.852381235147,4.35017462060976,337.298674676133));
#50130=CARTESIAN_POINT('Ctrl Pts',(158.84461998022,4.41074078967135,337.175901824263));
#50131=CARTESIAN_POINT('Ctrl Pts',(158.836846309816,4.471403844865,337.052932575841));
#50132=CARTESIAN_POINT('Ctrl Pts',(158.829072639411,4.52685628584907,336.927554823908));
#50133=CARTESIAN_POINT('Ctrl Pts',(158.821298969006,4.57692746455687,336.800254994906));
#50134=CARTESIAN_POINT('Ctrl Pts',(158.813887164829,4.62466781784968,336.678881003571));
#50135=CARTESIAN_POINT('Ctrl Pts',(158.806475360652,4.66751653519789,336.555760125294));
#50136=CARTESIAN_POINT('Ctrl Pts',(158.799063556475,4.70536867922647,336.431324091551));
#50137=CARTESIAN_POINT('Ctrl Pts',(158.791288477697,4.74507606958935,336.300789077119));
#50138=CARTESIAN_POINT('Ctrl Pts',(158.783513398918,4.77941019099073,336.168394213356));
#50139=CARTESIAN_POINT('Ctrl Pts',(158.77573832014,4.80819525881478,336.034621387567));
#50140=CARTESIAN_POINT('Ctrl Pts',(158.767972809091,4.83694490478029,335.901013177757));
#50141=CARTESIAN_POINT('Ctrl Pts',(158.760207298042,4.86015900241358,335.766030758294));
#50142=CARTESIAN_POINT('Ctrl Pts',(158.752441786993,4.8777111325648,335.630172333377));
#50143=CARTESIAN_POINT('Ctrl Pts',(158.744683975471,4.89524585972788,335.494448612483));
#50144=CARTESIAN_POINT('Ctrl Pts',(158.736926163948,4.90712974154233,335.357850999779));
#50145=CARTESIAN_POINT('Ctrl Pts',(158.729168352426,4.91328721207829,335.220888736988));
#50146=CARTESIAN_POINT('Ctrl Pts',(158.721416378903,4.91944004892239,335.084029542642));
#50147=CARTESIAN_POINT('Ctrl Pts',(158.71366440538,4.91987503446681,334.946806633317));
#50148=CARTESIAN_POINT('Ctrl Pts',(158.705912431857,4.91456836825406,334.809734879033));
#50149=CARTESIAN_POINT('Ctrl Pts',(158.6981637413,4.90926394941759,334.672721174718));
#50150=CARTESIAN_POINT('Ctrl Pts',(158.690415050742,4.89822273018065,334.535858887892));
#50151=CARTESIAN_POINT('Ctrl Pts',(158.682666360184,4.88147301181509,334.399663180022));
#50152=CARTESIAN_POINT('Ctrl Pts',(158.674919281806,4.86472677836834,334.263495808807));
#50153=CARTESIAN_POINT('Ctrl Pts',(158.667172203429,4.84227445589549,334.127995128398));
#50154=CARTESIAN_POINT('Ctrl Pts',(158.659425125051,4.81419621043001,333.99367107267));
#50155=CARTESIAN_POINT('Ctrl Pts',(158.651677981745,4.78611772964179,333.859345891177));
#50156=CARTESIAN_POINT('Ctrl Pts',(158.643930838439,4.75241331179268,333.726197736639));
#50157=CARTESIAN_POINT('Ctrl Pts',(158.636183695133,4.71321415177927,333.594725855227));
#50158=CARTESIAN_POINT('Ctrl Pts',(158.628434810105,4.67400617896248,333.463224416145));
#50159=CARTESIAN_POINT('Ctrl Pts',(158.620685925077,4.62930111746466,333.333400374607));
#50160=CARTESIAN_POINT('Ctrl Pts',(158.612937040049,4.57927976624232,333.205736952121));
#50161=CARTESIAN_POINT('Ctrl Pts',(158.605179930274,4.52920532184094,333.077938026359));
#50162=CARTESIAN_POINT('Ctrl Pts',(158.5974228205,4.47380345858585,332.952304665247));
#50163=CARTESIAN_POINT('Ctrl Pts',(158.589665710725,4.41330302220074,332.829299768109));
#50164=CARTESIAN_POINT('Ctrl Pts',(158.581904455799,4.35277025631687,332.706229141086));
#50165=CARTESIAN_POINT('Ctrl Pts',(158.574143200873,4.28713367541245,332.585790119804));
#50166=CARTESIAN_POINT('Ctrl Pts',(158.566381945946,4.21666719439612,332.468419301266));
#50167=CARTESIAN_POINT('Ctrl Pts',(158.558608275542,4.14608798997516,332.350860727669));
#50168=CARTESIAN_POINT('Ctrl Pts',(158.550834605137,4.0706636612342,332.236380491274));
#50169=CARTESIAN_POINT('Ctrl Pts',(158.543060934732,3.99071090708656,332.125385326942));
#50170=CARTESIAN_POINT('Ctrl Pts',(158.535649130555,3.91447997287979,332.019557014213));
#50171=CARTESIAN_POINT('Ctrl Pts',(158.528237326378,3.83413289928455,331.916896841748));
#50172=CARTESIAN_POINT('Ctrl Pts',(158.520825522201,3.74997595087325,331.817726688298));
#50173=CARTESIAN_POINT('Ctrl Pts',(158.513050443423,3.6616942197298,331.713695910215));
#50174=CARTESIAN_POINT('Ctrl Pts',(158.505275364644,3.56894071745207,331.613177157444));
#50175=CARTESIAN_POINT('Ctrl Pts',(158.497500285866,3.47202554621446,331.51657902789));
#50176=CARTESIAN_POINT('Ctrl Pts',(158.489734774817,3.37522963526517,331.420099768485));
#50177=CARTESIAN_POINT('Ctrl Pts',(158.481969263768,3.27428251926863,331.327531806073));
#50178=CARTESIAN_POINT('Ctrl Pts',(158.474203752719,3.16953473610921,331.239251056093));
#50179=CARTESIAN_POINT('Ctrl Pts',(158.466445941196,3.06489081068179,331.151057836734));
#50180=CARTESIAN_POINT('Ctrl Pts',(158.458688129674,2.95645401432336,331.067143620781));
#50181=CARTESIAN_POINT('Ctrl Pts',(158.450930318152,2.84461168620243,330.987847533154));
#50182=CARTESIAN_POINT('Ctrl Pts',(158.443178344629,2.73285352297982,330.908611118347));
#50183=CARTESIAN_POINT('Ctrl Pts',(158.435426371106,2.61769524664332,330.833986139638));
#50184=CARTESIAN_POINT('Ctrl Pts',(158.427674397583,2.4995569425833,330.76427123705));
#50185=CARTESIAN_POINT('Ctrl Pts',(158.419925707025,2.3814686701653,330.694585858765));
#50186=CARTESIAN_POINT('Ctrl Pts',(158.412177016468,2.26040321607023,330.629806619017));
#50187=CARTESIAN_POINT('Ctrl Pts',(158.40442832591,2.13680910600832,330.570188502094));
#50188=CARTESIAN_POINT('Ctrl Pts',(158.396681247532,2.01324071073345,330.510582789218));
#50189=CARTESIAN_POINT('Ctrl Pts',(158.388934169154,1.88714505779272,330.456136232988));
#50190=CARTESIAN_POINT('Ctrl Pts',(158.381187090777,1.75899434390213,330.407057374556));
#50191=CARTESIAN_POINT('Ctrl Pts',(158.373439947471,1.63084255598512,330.357978104796));
#50192=CARTESIAN_POINT('Ctrl Pts',(158.365692804165,1.50063603778561,330.314266762358));
#50193=CARTESIAN_POINT('Ctrl Pts',(158.357945660859,1.36886561314595,330.276083193403));
#50194=CARTESIAN_POINT('Ctrl Pts',(158.350196775831,1.23706556371764,330.237891039972));
#50195=CARTESIAN_POINT('Ctrl Pts',(158.342447890803,1.10370128356213,330.205229241749));
#50196=CARTESIAN_POINT('Ctrl Pts',(158.334699005775,0.9692769646432,330.178207259918));
#50197=CARTESIAN_POINT('Ctrl Pts',(158.326941896,0.834709966362778,330.151156596676));
#50198=CARTESIAN_POINT('Ctrl Pts',(158.319184786225,0.699081065567712,330.129757784895));
#50199=CARTESIAN_POINT('Ctrl Pts',(158.311427676451,0.562903365726845,330.114068884711));
#50200=CARTESIAN_POINT('Ctrl Pts',(158.303666421524,0.426652896877232,330.098371600879));
#50201=CARTESIAN_POINT('Ctrl Pts',(158.295905166598,0.289853434273793,330.088390336852));
#50202=CARTESIAN_POINT('Ctrl Pts',(158.288143911672,0.153020352724308,330.084131019428));
#50203=CARTESIAN_POINT('Ctrl Pts',(158.280370241267,0.0159683828383288,
330.079864888484));
#50204=CARTESIAN_POINT('Ctrl Pts',(158.272596570863,-0.121116922403505,
330.081338990842));
#50205=CARTESIAN_POINT('Ctrl Pts',(158.264822900458,-0.257722147026157,
330.088507115201));
#50206=CARTESIAN_POINT('Ctrl Pts',(158.257411096281,-0.387968365575321,
330.095341561646));
#50207=CARTESIAN_POINT('Ctrl Pts',(158.249999292104,-0.517777906594161,
330.107351820001));
#50208=CARTESIAN_POINT('Ctrl Pts',(158.242587487927,-0.64671435804053,330.124454532916));
#50209=CARTESIAN_POINT('Ctrl Pts',(158.234812409149,-0.781970369055944,
330.142395500737));
#50210=CARTESIAN_POINT('Ctrl Pts',(158.22703733037,-0.916692975011703,330.165997434722));
#50211=CARTESIAN_POINT('Ctrl Pts',(158.219262251592,-1.05037076313152,330.195220679109));
#50212=CARTESIAN_POINT('Ctrl Pts',(158.211496740543,-1.18388405222312,330.224407962434));
#50213=CARTESIAN_POINT('Ctrl Pts',(158.203731229494,-1.31635470347679,330.259202709878));
#50214=CARTESIAN_POINT('Ctrl Pts',(158.195965718445,-1.4472769054165,330.29951357607));
#50215=CARTESIAN_POINT('Ctrl Pts',(158.188207906923,-1.57806929761172,330.339784473921));
#50216=CARTESIAN_POINT('Ctrl Pts',(158.1804500954,-1.70731592464961,330.385560492128));
#50217=CARTESIAN_POINT('Ctrl Pts',(158.172692283878,-1.83452199770111,330.436699428873));
#50218=CARTESIAN_POINT('Ctrl Pts',(158.164940310355,-1.96163234414888,330.487799881946));
#50219=CARTESIAN_POINT('Ctrl Pts',(158.157188336832,-2.08670483190564,330.544255075352));
#50220=CARTESIAN_POINT('Ctrl Pts',(158.149436363309,-2.2092609958955,330.605873361575));
#50221=CARTESIAN_POINT('Ctrl Pts',(158.141687672752,-2.33176525727679,330.667465552418));
#50222=CARTESIAN_POINT('Ctrl Pts',(158.133938982194,-2.45175496592983,330.734216311925));
#50223=CARTESIAN_POINT('Ctrl Pts',(158.126190291636,-2.56877297713006,330.805886451887));
#50224=CARTESIAN_POINT('Ctrl Pts',(158.118443213258,-2.68576664175569,330.877541680277));
#50225=CARTESIAN_POINT('Ctrl Pts',(158.110696134881,-2.79978950562923,330.954114049249));
#50226=CARTESIAN_POINT('Ctrl Pts',(158.102949056503,-2.91041066930885,331.035319332093));
#50227=CARTESIAN_POINT('Ctrl Pts',(158.095201913197,-3.02103276010031,331.116525295516));
#50228=CARTESIAN_POINT('Ctrl Pts',(158.087454769891,-3.12825277874338,331.202364018954));
#50229=CARTESIAN_POINT('Ctrl Pts',(158.079707626585,-3.23167069424558,331.292509260099));
#50230=CARTESIAN_POINT('Ctrl Pts',(158.071958741557,-3.33511186029055,331.382674767807));
#50231=CARTESIAN_POINT('Ctrl Pts',(158.064209856529,-3.43474892765857,331.477148463039));
#50232=CARTESIAN_POINT('Ctrl Pts',(158.056460971501,-3.53021700090189,331.575565595745));
#50233=CARTESIAN_POINT('Ctrl Pts',(158.048703861726,-3.62578640494471,331.674087189413));
#50234=CARTESIAN_POINT('Ctrl Pts',(158.040946751952,-3.71717770289908,331.776560300689));
#50235=CARTESIAN_POINT('Ctrl Pts',(158.033189642177,-3.80406440103096,331.88258486959));
#50236=CARTESIAN_POINT('Ctrl Pts',(158.025428387251,-3.89099752863613,331.98866609463));
#50237=CARTESIAN_POINT('Ctrl Pts',(158.017667132325,-3.97342102526369,332.098302246532));
#50238=CARTESIAN_POINT('Ctrl Pts',(158.009905877398,-4.05105100806086,332.211063142954));
#50239=CARTESIAN_POINT('Ctrl Pts',(158.002132206994,-4.12880517353106,332.324004420062));
#50240=CARTESIAN_POINT('Ctrl Pts',(157.994358536589,-4.20175029402894,332.440080099197));
#50241=CARTESIAN_POINT('Ctrl Pts',(157.986584866184,-4.26964739078003,332.558833430324));
#50242=CARTESIAN_POINT('Ctrl Pts',(157.979173062007,-4.33438386134288,332.672058765317));
#50243=CARTESIAN_POINT('Ctrl Pts',(157.97176125783,-4.39453156998078,332.787717817673));
#50244=CARTESIAN_POINT('Ctrl Pts',(157.964349453653,-4.44992444607144,332.905398489747));
#50245=CARTESIAN_POINT('Ctrl Pts',(157.955919680237,-4.51292521931634,333.039241934245));
#50246=CARTESIAN_POINT('Ctrl Pts',(157.947489906821,-4.56994996202602,333.176070695699));
#50247=CARTESIAN_POINT('Ctrl Pts',(157.939060133405,-4.62072962745642,333.315351439485));
#50248=CARTESIAN_POINT('Ctrl Pts',(157.930658840621,-4.67133772991915,333.454161612668));
#50249=CARTESIAN_POINT('Ctrl Pts',(157.922257547836,-4.71574273886886,333.595406978395));
#50250=CARTESIAN_POINT('Ctrl Pts',(157.913856255052,-4.75372361378086,333.738534635322));
#50251=CARTESIAN_POINT('Ctrl Pts',(157.905472365055,-4.79162581352958,333.88136581167));
#50252=CARTESIAN_POINT('Ctrl Pts',(157.897088475058,-4.82313033157454,334.026071233454));
#50253=CARTESIAN_POINT('Ctrl Pts',(157.88870458506,-4.8480647726888,334.172080304429));
#50254=CARTESIAN_POINT('Ctrl Pts',(157.880348513148,-4.87291648032184,334.317604911419));
#50255=CARTESIAN_POINT('Ctrl Pts',(157.871992441236,-4.89124153432854,334.464424261689));
#50256=CARTESIAN_POINT('Ctrl Pts',(157.863636369324,-4.90291802749534,334.611956345032));
#50257=CARTESIAN_POINT('Ctrl Pts',(157.85636337173,-4.91308106912587,334.740366021073));
#50258=CARTESIAN_POINT('Ctrl Pts',(157.849090374136,-4.91820806567256,334.869315271384));
#50259=CARTESIAN_POINT('Ctrl Pts',(157.841817376542,-4.91824974369148,334.99841217802));
#50260=CARTESIAN_POINT('',(156.091817376458,-4.9182479770399,335.004460811911));
#50261=CARTESIAN_POINT('Ctrl Pts',(157.841817376508,-4.91824974369168,334.998412178619));
#50262=CARTESIAN_POINT('Ctrl Pts',(157.833875574543,-4.91829525428665,335.139380473123));
#50263=CARTESIAN_POINT('Ctrl Pts',(157.825933772579,-4.91227570213308,335.280298249976));
#50264=CARTESIAN_POINT('Ctrl Pts',(157.817991970614,-4.90023038948937,335.420624764398));
#50265=CARTESIAN_POINT('Ctrl Pts',(157.810045362692,-4.88817778766127,335.561036196985));
#50266=CARTESIAN_POINT('Ctrl Pts',(157.80209875477,-4.87009218828604,335.700855292861));
#50267=CARTESIAN_POINT('Ctrl Pts',(157.794152146848,-4.84606460538666,335.839548034908));
#50268=CARTESIAN_POINT('Ctrl Pts',(157.786199405004,-4.82201847579423,335.978347832739));
#50269=CARTESIAN_POINT('Ctrl Pts',(157.778246663161,-4.79202128248692,336.116019187093));
#50270=CARTESIAN_POINT('Ctrl Pts',(157.770293921318,-4.75621479583,336.252039886916));
#50271=CARTESIAN_POINT('Ctrl Pts',(157.762327969214,-4.72034883119262,336.38828653006));
#50272=CARTESIAN_POINT('Ctrl Pts',(157.75436201711,-4.67865438582672,336.522876689614));
#50273=CARTESIAN_POINT('Ctrl Pts',(157.746396065006,-4.63132295370721,336.655303827388));
#50274=CARTESIAN_POINT('Ctrl Pts',(157.738422786762,-4.58394799173754,336.787852755972));
#50275=CARTESIAN_POINT('Ctrl Pts',(157.730449508518,-4.53092584125024,336.918234360921));
#50276=CARTESIAN_POINT('Ctrl Pts',(157.722476230274,-4.47249532858759,337.045963977753));
#50277=CARTESIAN_POINT('Ctrl Pts',(157.714488398953,-4.41395816673132,337.173926730664));
#50278=CARTESIAN_POINT('Ctrl Pts',(157.706500567633,-4.34999308182935,337.299227500727));
#50279=CARTESIAN_POINT('Ctrl Pts',(157.698512736313,-4.28088437930802,337.421407027638));
#50280=CARTESIAN_POINT('Ctrl Pts',(157.694378964002,-4.24512002356409,337.484635997445));
#50281=CARTESIAN_POINT('Ctrl Pts',(157.69024519169,-4.20797883152376,337.547029537613));
#50282=CARTESIAN_POINT('Ctrl Pts',(157.686111419379,-4.16950455071622,337.608527336268));
#50283=CARTESIAN_POINT('Ctrl Pts',(157.678336340601,-4.09713951904733,337.724196558768));
#50284=CARTESIAN_POINT('Ctrl Pts',(157.670561261822,-4.0198431950545,337.837034983697));
#50285=CARTESIAN_POINT('Ctrl Pts',(157.662786183044,-3.93786354806871,337.946593582307));
#50286=CARTESIAN_POINT('Ctrl Pts',(157.655020671995,-3.85598478225767,338.056017362086));
#50287=CARTESIAN_POINT('Ctrl Pts',(157.647255160946,-3.76943439236382,338.16216903613));
#50288=CARTESIAN_POINT('Ctrl Pts',(157.639489649897,-3.67850507197608,338.264626088535));
#50289=CARTESIAN_POINT('Ctrl Pts',(157.631731838374,-3.58766590827436,338.366981554475));
#50290=CARTESIAN_POINT('Ctrl Pts',(157.623974026852,-3.49245671213409,338.465649398344));
#50291=CARTESIAN_POINT('Ctrl Pts',(157.61621621533,-3.39321189705664,338.5602382061));
#50292=CARTESIAN_POINT('Ctrl Pts',(157.608464241807,-3.29404176684969,338.654755832778));
#50293=CARTESIAN_POINT('Ctrl Pts',(157.600712268284,-3.19084234437671,338.745200264654));
#50294=CARTESIAN_POINT('Ctrl Pts',(157.592960294761,-3.08398628283511,338.831215429832));
#50295=CARTESIAN_POINT('Ctrl Pts',(157.585211604203,-2.97717547489891,338.917194167538));
#50296=CARTESIAN_POINT('Ctrl Pts',(157.577462913646,-2.86671141177747,338.998747124787));
#50297=CARTESIAN_POINT('Ctrl Pts',(157.569714223088,-2.75300118246612,339.075557330211));
#50298=CARTESIAN_POINT('Ctrl Pts',(157.56196714471,-2.63931461151771,339.152351554631));
#50299=CARTESIAN_POINT('Ctrl Pts',(157.554220066332,-2.52238354148038,339.224404771324));
#50300=CARTESIAN_POINT('Ctrl Pts',(157.546472987955,-2.40264517940735,339.291442555175));
#50301=CARTESIAN_POINT('Ctrl Pts',(157.538725844649,-2.28290581381164,339.358480900868));
#50302=CARTESIAN_POINT('Ctrl Pts',(157.530978701343,-2.16035945031149,339.420503538931));
#50303=CARTESIAN_POINT('Ctrl Pts',(157.523231558037,-2.03546874738785,339.477281545861));
#50304=CARTESIAN_POINT('Ctrl Pts',(157.515482673009,-1.91054996638286,339.534072317693));
#50305=CARTESIAN_POINT('Ctrl Pts',(157.507733787981,-1.78328615292839,339.585615950371));
#50306=CARTESIAN_POINT('Ctrl Pts',(157.499984902953,-1.65416045643702,339.631731452369));
#50307=CARTESIAN_POINT('Ctrl Pts',(157.492227793178,-1.5248977045971,339.677895901837));
#50308=CARTESIAN_POINT('Ctrl Pts',(157.484470683404,-1.39376949071649,339.71862057987));
#50309=CARTESIAN_POINT('Ctrl Pts',(157.476713573629,-1.26127519151621,339.75377407475));
#50310=CARTESIAN_POINT('Ctrl Pts',(157.468952318703,-1.12871009159858,339.788946354534));
#50311=CARTESIAN_POINT('Ctrl Pts',(157.461191063776,-0.994777833259547,
339.818541434806));
#50312=CARTESIAN_POINT('Ctrl Pts',(157.45342980885,-0.859987555252061,339.842479165398));
#50313=CARTESIAN_POINT('Ctrl Pts',(157.445656138446,-0.724981656728042,
339.866455188557));
#50314=CARTESIAN_POINT('Ctrl Pts',(157.437882468041,-0.589115383350312,
339.884755725418));
#50315=CARTESIAN_POINT('Ctrl Pts',(157.430108797636,-0.45290345059257,339.897352501806));
#50316=CARTESIAN_POINT('Ctrl Pts',(157.422696993459,-0.323032216075101,
339.909362895222));
#50317=CARTESIAN_POINT('Ctrl Pts',(157.415285189282,-0.192847066256581,
339.91618858292));
#50318=CARTESIAN_POINT('Ctrl Pts',(157.407873385105,-0.0627918709568618,
339.917849148097));
#50319=CARTESIAN_POINT('Ctrl Pts',(157.400098306327,0.0736377168784359,
339.91959110252));
#50320=CARTESIAN_POINT('Ctrl Pts',(157.392323227548,0.210355431878305,339.915654321027));
#50321=CARTESIAN_POINT('Ctrl Pts',(157.38454814877,0.346849485754007,339.906004331096));
#50322=CARTESIAN_POINT('Ctrl Pts',(157.376782637721,0.483175575006731,339.896366216092));
#50323=CARTESIAN_POINT('Ctrl Pts',(157.369017126672,0.619278164588814,339.881028908566));
#50324=CARTESIAN_POINT('Ctrl Pts',(157.361251615623,0.754643558566898,339.860009893201));
#50325=CARTESIAN_POINT('Ctrl Pts',(157.353493804101,0.889874737363047,339.839011718251));
#50326=CARTESIAN_POINT('Ctrl Pts',(157.345735992578,1.02436979139278,339.812343105895));
#50327=CARTESIAN_POINT('Ctrl Pts',(157.337978181056,1.1576186019034,339.780073454982));
#50328=CARTESIAN_POINT('Ctrl Pts',(157.330226207533,1.29076713845844,339.747828088005));
#50329=CARTESIAN_POINT('Ctrl Pts',(157.32247423401,1.42267091985141,339.709990163773));
#50330=CARTESIAN_POINT('Ctrl Pts',(157.314722260487,1.55282885360297,339.666680363376));
#50331=CARTESIAN_POINT('Ctrl Pts',(157.30697356993,1.68293166539236,339.623388904705));
#50332=CARTESIAN_POINT('Ctrl Pts',(157.299224879372,1.81128972998111,339.574630302054));
#50333=CARTESIAN_POINT('Ctrl Pts',(157.291476188814,1.93741620016834,339.520575353849));
#50334=CARTESIAN_POINT('Ctrl Pts',(157.283729110436,2.06351642868999,339.466531652227));
#50335=CARTESIAN_POINT('Ctrl Pts',(157.275982032059,2.18738562729551,339.407193950783));
#50336=CARTESIAN_POINT('Ctrl Pts',(157.268234953681,2.30855642822807,339.342781399079));
#50337=CARTESIAN_POINT('Ctrl Pts',(157.260487810375,2.42972824468856,339.278368307536));
#50338=CARTESIAN_POINT('Ctrl Pts',(157.252740667069,2.54820127322909,339.208880464371));
#50339=CARTESIAN_POINT('Ctrl Pts',(157.244993523763,2.66353263614156,339.134583045327));
#50340=CARTESIAN_POINT('Ctrl Pts',(157.237244638735,2.778889927993,339.060268922647));
#50341=CARTESIAN_POINT('Ctrl Pts',(157.229495753707,2.89110382020343,338.981143284074));
#50342=CARTESIAN_POINT('Ctrl Pts',(157.221746868679,2.99976065326719,338.897514475356));
#50343=CARTESIAN_POINT('Ctrl Pts',(157.213989758904,3.10853281581625,338.813796902157));
#50344=CARTESIAN_POINT('Ctrl Pts',(157.20623264913,3.21374006706319,338.725566849672));
#50345=CARTESIAN_POINT('Ctrl Pts',(157.198475539355,3.31500165869355,338.633173140019));
#50346=CARTESIAN_POINT('Ctrl Pts',(157.190714284429,3.41631736128068,338.540730058123));
#50347=CARTESIAN_POINT('Ctrl Pts',(157.182953029503,3.51368292568357,338.444119160867));
#50348=CARTESIAN_POINT('Ctrl Pts',(157.175191774576,3.60675542772115,338.343725220036));
#50349=CARTESIAN_POINT('Ctrl Pts',(157.167418104172,3.69997681542977,338.243170681618));
#50350=CARTESIAN_POINT('Ctrl Pts',(157.159644433767,3.78889116383087,338.138821304335));
#50351=CARTESIAN_POINT('Ctrl Pts',(157.151870763362,3.87319615449022,338.031094622631));
#50352=CARTESIAN_POINT('Ctrl Pts',(157.144458959185,3.95357672755246,337.928382643877));
#50353=CARTESIAN_POINT('Ctrl Pts',(157.137047155008,4.02976724854739,337.822600945287));
#50354=CARTESIAN_POINT('Ctrl Pts',(157.129635350831,4.10154398197392,337.714133384053));
#50355=CARTESIAN_POINT('Ctrl Pts',(157.121860272053,4.17683870691696,337.600349504536));
#50356=CARTESIAN_POINT('Ctrl Pts',(157.114085193274,4.24751398381902,337.48325024289));
#50357=CARTESIAN_POINT('Ctrl Pts',(157.106310114496,4.31326386599218,337.363247317744));
#50358=CARTESIAN_POINT('Ctrl Pts',(157.098544603447,4.37893283874944,337.243392063839));
#50359=CARTESIAN_POINT('Ctrl Pts',(157.090779092398,4.43968829043148,337.12064059548));
#50360=CARTESIAN_POINT('Ctrl Pts',(157.083013581349,4.49526693393644,336.995434352505));
#50361=CARTESIAN_POINT('Ctrl Pts',(157.075255769826,4.55079047105438,336.870352251885));
#50362=CARTESIAN_POINT('Ctrl Pts',(157.067497958304,4.60114725703393,336.742820575235));
#50363=CARTESIAN_POINT('Ctrl Pts',(157.059740146782,4.64611959632103,336.613305847997));
#50364=CARTESIAN_POINT('Ctrl Pts',(157.051988173259,4.69105809249678,336.483888584699));
#50365=CARTESIAN_POINT('Ctrl Pts',(157.044236199736,4.73062007952204,336.35249160894));
#50366=CARTESIAN_POINT('Ctrl Pts',(157.036484226213,4.76463587080769,336.219601607539));
#50367=CARTESIAN_POINT('Ctrl Pts',(157.028735535655,4.7986372563856,336.086767885133));
#50368=CARTESIAN_POINT('Ctrl Pts',(157.020986845098,4.82709702113057,335.952442772559));
#50369=CARTESIAN_POINT('Ctrl Pts',(157.01323815454,4.84989533212657,335.817128098842));
#50370=CARTESIAN_POINT('Ctrl Pts',(157.005491076162,4.87268889974354,335.681841578473));
#50371=CARTESIAN_POINT('Ctrl Pts',(156.997743997785,4.88982329166342,335.545566291684));
#50372=CARTESIAN_POINT('Ctrl Pts',(156.989996919407,4.90122987591784,335.408813852395));
#50373=CARTESIAN_POINT('Ctrl Pts',(156.982249776101,4.9126365557704,335.27206026699));
#50374=CARTESIAN_POINT('Ctrl Pts',(156.974502632795,4.91831529971869,335.134829910631));
#50375=CARTESIAN_POINT('Ctrl Pts',(156.966755489489,4.91824943316335,334.997638710442));
#50376=CARTESIAN_POINT('Ctrl Pts',(156.959006604461,4.91818355179981,334.860416666758));
#50377=CARTESIAN_POINT('Ctrl Pts',(156.951257719433,4.91237049015884,334.72323418756));
#50378=CARTESIAN_POINT('Ctrl Pts',(156.943508834405,4.90084568786444,334.586605991528));
#50379=CARTESIAN_POINT('Ctrl Pts',(156.93575172463,4.8893086530258,334.449832776917));
#50380=CARTESIAN_POINT('Ctrl Pts',(156.927994614856,4.8720478000262,334.313615410806));
#50381=CARTESIAN_POINT('Ctrl Pts',(156.920237505081,4.84915041606605,334.17846284024));
#50382=CARTESIAN_POINT('Ctrl Pts',(156.912476250155,4.82624079647601,334.043238048461));
#50383=CARTESIAN_POINT('Ctrl Pts',(156.904714995229,4.79768872560381,333.909079568115));
#50384=CARTESIAN_POINT('Ctrl Pts',(156.896953740302,4.76363219029968,333.776483993549));
#50385=CARTESIAN_POINT('Ctrl Pts',(156.889180069898,4.72952117563804,333.643676309278));
#50386=CARTESIAN_POINT('Ctrl Pts',(156.881406399493,4.68988821390836,333.512436901189));
#50387=CARTESIAN_POINT('Ctrl Pts',(156.873632729088,4.64492081688073,333.38324594715));
#50388=CARTESIAN_POINT('Ctrl Pts',(156.866220924911,4.60204666300323,333.260068863102));
#50389=CARTESIAN_POINT('Ctrl Pts',(156.858809120734,4.55432363862722,333.138754081685));
#50390=CARTESIAN_POINT('Ctrl Pts',(156.851397316557,4.50195346133741,333.019697474008));
#50391=CARTESIAN_POINT('Ctrl Pts',(156.843622237779,4.44701646565601,332.894805547336));
#50392=CARTESIAN_POINT('Ctrl Pts',(156.835847159,4.38679164601235,332.772004069567));
#50393=CARTESIAN_POINT('Ctrl Pts',(156.828072080222,4.32145966007909,332.651773122373));
#50394=CARTESIAN_POINT('Ctrl Pts',(156.820306569173,4.25620806931384,332.531690127014));
#50395=CARTESIAN_POINT('Ctrl Pts',(156.812541058124,4.18586200183611,332.414171708528));
#50396=CARTESIAN_POINT('Ctrl Pts',(156.804775547075,4.11065019406275,332.29967815908));
#50397=CARTESIAN_POINT('Ctrl Pts',(156.797017735553,4.03551295901557,332.185298130319));
#50398=CARTESIAN_POINT('Ctrl Pts',(156.78925992403,3.95551979771654,332.073937326672));
#50399=CARTESIAN_POINT('Ctrl Pts',(156.781502112508,3.87094521380705,331.96603127666));
#50400=CARTESIAN_POINT('Ctrl Pts',(156.773750138985,3.78643427495443,331.858206429374));
#50401=CARTESIAN_POINT('Ctrl Pts',(156.765998165462,3.69734901605317,331.753831467327));
#50402=CARTESIAN_POINT('Ctrl Pts',(156.758246191939,3.60400687528268,331.653312457755));
#50403=CARTESIAN_POINT('Ctrl Pts',(156.750497501382,3.51070426496394,331.552836018044));
#50404=CARTESIAN_POINT('Ctrl Pts',(156.742748810824,3.4131486238242,331.456212568721));
#50405=CARTESIAN_POINT('Ctrl Pts',(156.735000120266,3.31169710213056,331.363814448321));
#50406=CARTESIAN_POINT('Ctrl Pts',(156.727253041889,3.21026668827332,331.271435552122));
#50407=CARTESIAN_POINT('Ctrl Pts',(156.719505963511,3.10494229494595,331.183280499254));
#50408=CARTESIAN_POINT('Ctrl Pts',(156.711758885133,2.99611700851296,331.099683867454));
#50409=CARTESIAN_POINT('Ctrl Pts',(156.704011741827,2.88729081001919,331.016086535033));
#50410=CARTESIAN_POINT('Ctrl Pts',(156.696264598521,2.77496396987199,330.937047937994));
#50411=CARTESIAN_POINT('Ctrl Pts',(156.688517455215,2.65956131861443,330.862861296134));
#50412=CARTESIAN_POINT('Ctrl Pts',(156.680768570187,2.54413272239081,330.788657975541));
#50413=CARTESIAN_POINT('Ctrl Pts',(156.673019685159,2.42562726776568,330.719308992068));
#50414=CARTESIAN_POINT('Ctrl Pts',(156.665270800131,2.30449697107282,330.655063087591));
#50415=CARTESIAN_POINT('Ctrl Pts',(156.657513690356,2.18323810543156,330.590748991847));
#50416=CARTESIAN_POINT('Ctrl Pts',(156.649756580582,2.05934917821337,330.531548978425));
#50417=CARTESIAN_POINT('Ctrl Pts',(156.641999470807,1.93330540995811,330.477665066105));
#50418=CARTESIAN_POINT('Ctrl Pts',(156.634238215881,1.80719428794308,330.423752359945));
#50419=CARTESIAN_POINT('Ctrl Pts',(156.626476960955,1.67892639580717,330.375161553746));
#50420=CARTESIAN_POINT('Ctrl Pts',(156.618715706028,1.54899400293614,330.332045347117));
#50421=CARTESIAN_POINT('Ctrl Pts',(156.610942035624,1.41885376058149,330.28886016861));
#50422=CARTESIAN_POINT('Ctrl Pts',(156.603168365219,1.28704407271883,330.251167197428));
#50423=CARTESIAN_POINT('Ctrl Pts',(156.595394694815,1.15407020453884,330.21906860272));
#50424=CARTESIAN_POINT('Ctrl Pts',(156.587982890637,1.02728630191402,330.188464205318));
#50425=CARTESIAN_POINT('Ctrl Pts',(156.58057108646,0.899444447246702,330.162945125377));
#50426=CARTESIAN_POINT('Ctrl Pts',(156.573159282283,0.770986697957244,330.142555962847));
#50427=CARTESIAN_POINT('Ctrl Pts',(156.565384203505,0.636232851719303,330.121167466726));
#50428=CARTESIAN_POINT('Ctrl Pts',(156.557609124726,0.500375363599819,330.105356876436));
#50429=CARTESIAN_POINT('Ctrl Pts',(156.549834045948,0.363915708752337,330.095232072827));
#50430=CARTESIAN_POINT('Ctrl Pts',(156.542068534899,0.227623976197869,330.085119728434));
#50431=CARTESIAN_POINT('Ctrl Pts',(156.53430302385,0.0907319373783311,330.080679277895));
#50432=CARTESIAN_POINT('Ctrl Pts',(156.526537512801,-0.0462495558042956,
330.08196746238));
#50433=CARTESIAN_POINT('Ctrl Pts',(156.518779701279,-0.183095231437924,
330.083254369627));
#50434=CARTESIAN_POINT('Ctrl Pts',(156.511021889757,-0.320029796588839,
330.090258604807));
#50435=CARTESIAN_POINT('Ctrl Pts',(156.503264078234,-0.456538456360242,
330.102985021427));
#50436=CARTESIAN_POINT('Ctrl Pts',(156.495512104711,-0.592944389036995,
330.115701861015));
#50437=CARTESIAN_POINT('Ctrl Pts',(156.487760131188,-0.728924666668749,
330.134132274779));
#50438=CARTESIAN_POINT('Ctrl Pts',(156.480008157665,-0.863966034639482,
330.158229068462));
#50439=CARTESIAN_POINT('Ctrl Pts',(156.472259467108,-0.998950212509602,
330.182315657138));
#50440=CARTESIAN_POINT('Ctrl Pts',(156.46451077655,-1.13299588757902,330.21206378435));
#50441=CARTESIAN_POINT('Ctrl Pts',(156.456762085992,-1.26559667792607,330.247374608564));
#50442=CARTESIAN_POINT('Ctrl Pts',(156.449015007615,-1.39816987957107,330.282678086066));
#50443=CARTESIAN_POINT('Ctrl Pts',(156.441267929237,-1.52929841697455,330.32354185797));
#50444=CARTESIAN_POINT('Ctrl Pts',(156.433520850859,-1.65848821499391,330.369816428777));
#50445=CARTESIAN_POINT('Ctrl Pts',(156.425773707553,-1.78767909574841,330.416091387408));
#50446=CARTESIAN_POINT('Ctrl Pts',(156.418026564247,-1.91493083672951,330.467777103585));
#50447=CARTESIAN_POINT('Ctrl Pts',(156.410279420942,-2.03976696297059,330.524675006296));
#50448=CARTESIAN_POINT('Ctrl Pts',(156.402530535914,-2.16463115502318,330.581585700863));
#50449=CARTESIAN_POINT('Ctrl Pts',(156.394781650885,-2.28707829606063,330.643710751659));
#50450=CARTESIAN_POINT('Ctrl Pts',(156.387032765857,-2.40665460175712,330.710804657008));
#50451=CARTESIAN_POINT('Ctrl Pts',(156.379275656083,-2.52635782698008,330.777969776522));
#50452=CARTESIAN_POINT('Ctrl Pts',(156.371518546308,-2.64318378850639,330.850114094315));
#50453=CARTESIAN_POINT('Ctrl Pts',(156.363761436533,-2.75670543533197,330.926947311253));
#50454=CARTESIAN_POINT('Ctrl Pts',(156.356000181607,-2.87028774449553,331.003821585404));
#50455=CARTESIAN_POINT('Ctrl Pts',(156.348238926681,-2.98056190651265,331.085389519002));
#50456=CARTESIAN_POINT('Ctrl Pts',(156.340477671755,-3.08713311781144,331.17131978674));
#50457=CARTESIAN_POINT('Ctrl Pts',(156.33270400135,-3.19387480831718,331.257387514901));
#50458=CARTESIAN_POINT('Ctrl Pts',(156.324930330945,-3.29690141726917,331.347831263932));
#50459=CARTESIAN_POINT('Ctrl Pts',(156.317156660541,-3.39585360046394,331.442281435145));
#50460=CARTESIAN_POINT('Ctrl Pts',(156.309744856364,-3.49019953572415,331.532334928163));
#50461=CARTESIAN_POINT('Ctrl Pts',(156.302333052187,-3.58084163759681,331.626030032698));
#50462=CARTESIAN_POINT('Ctrl Pts',(156.29492124801,-3.66750317839583,331.723019148827));
#50463=CARTESIAN_POINT('Ctrl Pts',(156.287219650529,-3.75755308909672,331.823800431571));
#50464=CARTESIAN_POINT('Ctrl Pts',(156.279518053048,-3.84360256713885,331.928471978928));
#50465=CARTESIAN_POINT('Ctrl Pts',(156.271816455568,-3.9252917545574,332.036679615009));
#50466=CARTESIAN_POINT('Ctrl Pts',(156.264127036115,-4.00685177226002,332.144716149503));
#50467=CARTESIAN_POINT('Ctrl Pts',(156.256437616662,-4.08406498868042,332.256277324793));
#50468=CARTESIAN_POINT('Ctrl Pts',(156.248748197208,-4.15660945517515,332.370973393127));
#50469=CARTESIAN_POINT('Ctrl Pts',(156.241065785242,-4.22908781077588,332.48556493716));
#50470=CARTESIAN_POINT('Ctrl Pts',(156.233383373276,-4.29690566474379,332.603285358931));
#50471=CARTESIAN_POINT('Ctrl Pts',(156.225700961309,-4.35978221692826,332.723713092895));
#50472=CARTESIAN_POINT('Ctrl Pts',(156.218023808879,-4.42261572254353,332.844058379579));
#50473=CARTESIAN_POINT('Ctrl Pts',(156.210346656448,-4.48051447069794,332.967106939896));
#50474=CARTESIAN_POINT('Ctrl Pts',(156.202669504018,-4.53324204575847,333.092409997649));
#50475=CARTESIAN_POINT('Ctrl Pts',(156.194995867573,-4.58594547262022,333.217655669052));
#50476=CARTESIAN_POINT('Ctrl Pts',(156.187322231128,-4.6334822839511,333.345153416556));
#50477=CARTESIAN_POINT('Ctrl Pts',(156.179648594683,-4.67566315401046,333.474432193336));
#50478=CARTESIAN_POINT('Ctrl Pts',(156.171974930537,-4.71784417634117,333.603711436808));
#50479=CARTESIAN_POINT('Ctrl Pts',(156.164301266391,-4.75466908259651,333.734771347252));
#50480=CARTESIAN_POINT('Ctrl Pts',(156.156627602244,-4.78599768438752,333.867123472069));
#50481=CARTESIAN_POINT('Ctrl Pts',(156.148954192266,-4.81732524851066,333.999471213111));
#50482=CARTESIAN_POINT('Ctrl Pts',(156.141280782287,-4.84315678410189,334.133110693588));
#50483=CARTESIAN_POINT('Ctrl Pts',(156.133607372308,-4.86340293630255,334.267541849889));
#50484=CARTESIAN_POINT('Ctrl Pts',(156.125929104274,-4.88366190639211,334.402058114887));
#50485=CARTESIAN_POINT('Ctrl Pts',(156.118250836241,-4.89832837372554,334.537366661299));
#50486=CARTESIAN_POINT('Ctrl Pts',(156.110572568207,-4.90736470654562,334.672960706565));
#50487=CARTESIAN_POINT('Ctrl Pts',(156.104320837641,-4.91472218844808,334.783362874567));
#50488=CARTESIAN_POINT('Ctrl Pts',(156.098069107074,-4.91834820572126,334.893954111272));
#50489=CARTESIAN_POINT('Ctrl Pts',(156.091817376508,-4.9182479770407,335.004460811032));
#50490=CARTESIAN_POINT('',(154.341817376458,-4.91824996390269,334.999404121525));
#50491=CARTESIAN_POINT('Ctrl Pts',(156.091817376458,-4.9182479770399,335.004460811911));
#50492=CARTESIAN_POINT('Ctrl Pts',(156.082140388515,-4.91809283408962,335.175512969368));
#50493=CARTESIAN_POINT('Ctrl Pts',(156.072463400572,-4.90901055079777,335.346167571306));
#50494=CARTESIAN_POINT('Ctrl Pts',(156.062786412629,-4.8911469239986,335.515620820331));
#50495=CARTESIAN_POINT('Ctrl Pts',(156.052937447765,-4.87296582945554,335.688085548563));
#50496=CARTESIAN_POINT('Ctrl Pts',(156.043088482901,-4.84568852631992,335.859305977571));
#50497=CARTESIAN_POINT('Ctrl Pts',(156.033239518037,-4.80951721499421,336.028458662842));
#50498=CARTESIAN_POINT('Ctrl Pts',(156.027720749936,-4.78924898560597,336.123241663542));
#50499=CARTESIAN_POINT('Ctrl Pts',(156.022201981836,-4.76618906848099,336.217375848896));
#50500=CARTESIAN_POINT('Ctrl Pts',(156.016683213735,-4.74037952019043,336.310719293769));
#50501=CARTESIAN_POINT('Ctrl Pts',(156.008908134957,-4.70401791420537,336.442225569104));
#50502=CARTESIAN_POINT('Ctrl Pts',(156.001133056179,-4.66212238829901,336.572425403022));
#50503=CARTESIAN_POINT('Ctrl Pts',(155.9933579774,-4.61480251546809,336.700817687387));
#50504=CARTESIAN_POINT('Ctrl Pts',(155.985592466351,-4.56754087275327,336.829051976872));
#50505=CARTESIAN_POINT('Ctrl Pts',(155.977826955302,-4.51486829833741,336.95548277928));
#50506=CARTESIAN_POINT('Ctrl Pts',(155.970061444253,-4.45694479432792,337.079621639341));
#50507=CARTESIAN_POINT('Ctrl Pts',(155.962303632731,-4.39907872164128,337.20363741536));
#50508=CARTESIAN_POINT('Ctrl Pts',(155.954545821209,-4.33597224442796,337.325365419439));
#50509=CARTESIAN_POINT('Ctrl Pts',(155.946788009687,-4.26783422348802,337.444335104548));
#50510=CARTESIAN_POINT('Ctrl Pts',(155.939036036164,-4.1997474785696,337.563215261196));
#50511=CARTESIAN_POINT('Ctrl Pts',(155.931284062641,-4.12663692004067,337.67934089268));
#50512=CARTESIAN_POINT('Ctrl Pts',(155.923532089118,-4.04875814139768,337.792264417093));
#50513=CARTESIAN_POINT('Ctrl Pts',(155.91578339856,-3.97091234446371,337.905140118327));
#50514=CARTESIAN_POINT('Ctrl Pts',(155.908034708002,-3.88830256520004,338.014816088564));
#50515=CARTESIAN_POINT('Ctrl Pts',(155.900286017445,-3.80122855609768,338.120872398354));
#50516=CARTESIAN_POINT('Ctrl Pts',(155.892538939067,-3.71417266347014,338.226906642243));
#50517=CARTESIAN_POINT('Ctrl Pts',(155.884791860689,-3.62265463636649,338.329322421744));
#50518=CARTESIAN_POINT('Ctrl Pts',(155.877044782311,-3.52701523089275,338.427731994125));
#50519=CARTESIAN_POINT('Ctrl Pts',(155.869297639006,-3.4313750238688,338.526142391273));
#50520=CARTESIAN_POINT('Ctrl Pts',(155.8615504957,-3.33161364199637,338.620546234025));
#50521=CARTESIAN_POINT('Ctrl Pts',(155.853803352394,-3.22810921533688,338.710592130153));
#50522=CARTESIAN_POINT('Ctrl Pts',(155.846054467366,-3.12458151868475,338.800658270511));
#50523=CARTESIAN_POINT('Ctrl Pts',(155.838305582338,-3.01730939756178,338.886364258134));
#50524=CARTESIAN_POINT('Ctrl Pts',(155.83055669731,-2.90670429490668,338.967398795744));
#50525=CARTESIAN_POINT('Ctrl Pts',(155.822799587535,-2.79598179485283,339.048519344249));
#50526=CARTESIAN_POINT('Ctrl Pts',(155.81504247776,-2.68191956226115,339.124958306648));
#50527=CARTESIAN_POINT('Ctrl Pts',(155.807285367986,-2.56495873655645,339.19644727624));
#50528=CARTESIAN_POINT('Ctrl Pts',(155.799524113059,-2.44793541072621,339.267974447252));
#50529=CARTESIAN_POINT('Ctrl Pts',(155.791762858133,-2.3280107470058,339.334546165208));
#50530=CARTESIAN_POINT('Ctrl Pts',(155.784001603207,-2.20564986441646,339.395940370171));
#50531=CARTESIAN_POINT('Ctrl Pts',(155.776227932802,-2.08309324429231,339.457432785854));
#50532=CARTESIAN_POINT('Ctrl Pts',(155.768454262398,-1.95809297420979,339.51373097739));
#50533=CARTESIAN_POINT('Ctrl Pts',(155.760680591993,-1.83113431666315,339.56466101445));
#50534=CARTESIAN_POINT('Ctrl Pts',(155.753268787816,-1.71008561516884,339.613220246032));
#50535=CARTESIAN_POINT('Ctrl Pts',(155.745856983639,-1.5872570201141,339.656899754762));
#50536=CARTESIAN_POINT('Ctrl Pts',(155.738445179462,-1.46307954419439,339.695591689006));
#50537=CARTESIAN_POINT('Ctrl Pts',(155.730670100683,-1.33281576027507,339.736180030204));
#50538=CARTESIAN_POINT('Ctrl Pts',(155.722895021905,-1.20065586920854,339.771407789666));
#50539=CARTESIAN_POINT('Ctrl Pts',(155.715119943126,-1.06708055975425,339.801095931295));
#50540=CARTESIAN_POINT('Ctrl Pts',(155.707354432077,-0.933669623222156,
339.830747539775));
#50541=CARTESIAN_POINT('Ctrl Pts',(155.699588921028,-0.79884711182609,339.85487301001));
#50542=CARTESIAN_POINT('Ctrl Pts',(155.691823409979,-0.663110364345369,
339.873342560009));
#50543=CARTESIAN_POINT('Ctrl Pts',(155.684065598457,-0.527508200244869,
339.891793797396));
#50544=CARTESIAN_POINT('Ctrl Pts',(155.676307786935,-0.39099398879215,339.904600222149));
#50545=CARTESIAN_POINT('Ctrl Pts',(155.668549975413,-0.254076449587683,
339.911682829771));
#50546=CARTESIAN_POINT('Ctrl Pts',(155.66079800189,-0.117261945173489,339.918760107506));
#50547=CARTESIAN_POINT('Ctrl Pts',(155.653046028367,0.0199548940762356,
339.920122121577));
#50548=CARTESIAN_POINT('Ctrl Pts',(155.645294054844,0.157059370680539,339.915741593756));
#50549=CARTESIAN_POINT('Ctrl Pts',(155.637545364286,0.294105783457671,339.911362921091));
#50550=CARTESIAN_POINT('Ctrl Pts',(155.629796673728,0.431039538372006,339.901246556007));
#50551=CARTESIAN_POINT('Ctrl Pts',(155.622047983171,0.56734529451731,339.885417318847));
#50552=CARTESIAN_POINT('Ctrl Pts',(155.614300904793,0.703622691111577,339.869591375092));
#50553=CARTESIAN_POINT('Ctrl Pts',(155.606553826415,0.839271960808397,339.848054968554));
#50554=CARTESIAN_POINT('Ctrl Pts',(155.598806748037,0.973782639789811,339.820884818469));
#50555=CARTESIAN_POINT('Ctrl Pts',(155.591059604731,1.10829444610027,339.793714440672));
#50556=CARTESIAN_POINT('Ctrl Pts',(155.583312461425,1.24166725952586,339.760910302544));
#50557=CARTESIAN_POINT('Ctrl Pts',(155.57556531812,1.37340095897385,339.722600223223));
#50558=CARTESIAN_POINT('Ctrl Pts',(155.567816433092,1.50516427495418,339.684281530984));
#50559=CARTESIAN_POINT('Ctrl Pts',(155.560067548063,1.63528736841611,339.640454543492));
#50560=CARTESIAN_POINT('Ctrl Pts',(155.552318663035,1.7632858074543,339.591296791074));
#50561=CARTESIAN_POINT('Ctrl Pts',(155.544561553261,1.89142010535819,339.54208686211));
#50562=CARTESIAN_POINT('Ctrl Pts',(155.536804443486,2.01742487853805,339.487535005933));
#50563=CARTESIAN_POINT('Ctrl Pts',(155.529047333711,2.14083569221801,339.427866935831));
#50564=CARTESIAN_POINT('Ctrl Pts',(155.521286078785,2.26431245269086,339.36816698102));
#50565=CARTESIAN_POINT('Ctrl Pts',(155.513524823859,2.38519214738026,339.303345549287));
#50566=CARTESIAN_POINT('Ctrl Pts',(155.505763568933,2.50303633875702,339.233673599767));
#50567=CARTESIAN_POINT('Ctrl Pts',(155.497989898528,2.62106904243464,339.163890197833));
#50568=CARTESIAN_POINT('Ctrl Pts',(155.490216228123,2.7360562114223,339.089240985787));
#50569=CARTESIAN_POINT('Ctrl Pts',(155.482442557719,2.84758898061532,339.010039907529));
#50570=CARTESIAN_POINT('Ctrl Pts',(155.475030753541,2.9539298725685,338.93452565852));
#50571=CARTESIAN_POINT('Ctrl Pts',(155.467618949364,3.05713050400697,338.85487396101));
#50572=CARTESIAN_POINT('Ctrl Pts',(155.460207145187,3.15686693448992,338.771388898062));
#50573=CARTESIAN_POINT('Ctrl Pts',(155.452432066409,3.2614917445309,338.683811983489));
#50574=CARTESIAN_POINT('Ctrl Pts',(155.44465698763,3.36263481940249,338.591739673597));
#50575=CARTESIAN_POINT('Ctrl Pts',(155.436881908852,3.45988547556214,338.495479303113));
#50576=CARTESIAN_POINT('Ctrl Pts',(155.429116397803,3.55701645859813,338.399337387144));
#50577=CARTESIAN_POINT('Ctrl Pts',(155.421350886754,3.65026427824316,338.299017937262));
#50578=CARTESIAN_POINT('Ctrl Pts',(155.413585375705,3.73925065950308,338.194868943776));
#50579=CARTESIAN_POINT('Ctrl Pts',(155.405827564183,3.82814881050685,338.090823214321));
#50580=CARTESIAN_POINT('Ctrl Pts',(155.398069752661,3.91279367929503,337.982955792774));
#50581=CARTESIAN_POINT('Ctrl Pts',(155.390311941139,3.99284353193543,337.871651718433));
#50582=CARTESIAN_POINT('Ctrl Pts',(155.382559967616,4.07283314452316,337.760431403939));
#50583=CARTESIAN_POINT('Ctrl Pts',(155.374807994093,4.14823439643133,337.645779900387));
#50584=CARTESIAN_POINT('Ctrl Pts',(155.36705602057,4.21874581647584,337.528115266056));
#50585=CARTESIAN_POINT('Ctrl Pts',(155.359307330012,4.28922737489214,337.410500462768));
#50586=CARTESIAN_POINT('Ctrl Pts',(155.351558639454,4.35482301971102,337.289875401283));
#50587=CARTESIAN_POINT('Ctrl Pts',(155.343809948897,4.41527474235423,337.166686874477));
#50588=CARTESIAN_POINT('Ctrl Pts',(155.336062870519,4.47571388751165,337.043523978072));
#50589=CARTESIAN_POINT('Ctrl Pts',(155.328315792141,4.53101106718072,336.917799027897));
#50590=CARTESIAN_POINT('Ctrl Pts',(155.320568713763,4.58095455494285,336.789982801048));
#50591=CARTESIAN_POINT('Ctrl Pts',(155.312821570458,4.63089846127948,336.662165502977));
#50592=CARTESIAN_POINT('Ctrl Pts',(155.305074427152,4.67548844395684,336.532257257341));
#50593=CARTESIAN_POINT('Ctrl Pts',(155.297327283846,4.7145613445959,336.400747796908));
#50594=CARTESIAN_POINT('Ctrl Pts',(155.289578398818,4.75364302965255,336.269208770356));
#50595=CARTESIAN_POINT('Ctrl Pts',(155.28182951379,4.78720505319706,336.136068187286));
#50596=CARTESIAN_POINT('Ctrl Pts',(155.274080628762,4.8151345503668,336.001829488668));
#50597=CARTESIAN_POINT('Ctrl Pts',(155.266323518987,4.84309369219341,335.867448307707));
#50598=CARTESIAN_POINT('Ctrl Pts',(155.258566409212,4.86540828544163,335.731967066184));
#50599=CARTESIAN_POINT('Ctrl Pts',(155.250809299438,4.88201680492332,335.595898463621));
#50600=CARTESIAN_POINT('Ctrl Pts',(155.243048044511,4.89863419946678,335.459757150348));
#50601=CARTESIAN_POINT('Ctrl Pts',(155.235286789585,4.90953941349002,335.323028240065));
#50602=CARTESIAN_POINT('Ctrl Pts',(155.227525534659,4.91472303860509,335.18622705578));
#50603=CARTESIAN_POINT('Ctrl Pts',(155.219751864255,4.91991495583101,335.049207034183));
#50604=CARTESIAN_POINT('Ctrl Pts',(155.21197819385,4.9193669959516,334.912114898628));
#50605=CARTESIAN_POINT('Ctrl Pts',(155.204204523445,4.91312190072349,334.775464365565));
#50606=CARTESIAN_POINT('Ctrl Pts',(155.196792719268,4.90716751618068,334.64517494769));
#50607=CARTESIAN_POINT('Ctrl Pts',(155.189380915091,4.89603448777209,334.515287231087));
#50608=CARTESIAN_POINT('Ctrl Pts',(155.181969110914,4.87980322267274,334.386238180975));
#50609=CARTESIAN_POINT('Ctrl Pts',(155.174194032135,4.86277641492058,334.250864052502));
#50610=CARTESIAN_POINT('Ctrl Pts',(155.166418953357,4.84008516665706,334.115985073058));
#50611=CARTESIAN_POINT('Ctrl Pts',(155.158643874579,4.81176567778183,333.982112911654));
#50612=CARTESIAN_POINT('Ctrl Pts',(155.15087836353,4.78348103784057,333.848405488468));
#50613=CARTESIAN_POINT('Ctrl Pts',(155.143112852481,4.7495820179819,333.715702796913));
#50614=CARTESIAN_POINT('Ctrl Pts',(155.135347341432,4.71015654437565,333.584511254027));
#50615=CARTESIAN_POINT('Ctrl Pts',(155.127589529909,4.67077016124126,333.453449787938));
#50616=CARTESIAN_POINT('Ctrl Pts',(155.119831718387,4.62586834063437,333.323896860725));
#50617=CARTESIAN_POINT('Ctrl Pts',(155.112073906865,4.57558993847664,333.196348210599));
#50618=CARTESIAN_POINT('Ctrl Pts',(155.104321933342,4.52534937241098,333.068895544877));
#50619=CARTESIAN_POINT('Ctrl Pts',(155.096569959819,4.46974042102218,332.943444516258));
#50620=CARTESIAN_POINT('Ctrl Pts',(155.088817986296,4.40895149507897,332.820474873616));
#50621=CARTESIAN_POINT('Ctrl Pts',(155.081069295738,4.34818831328198,332.69755730869));
#50622=CARTESIAN_POINT('Ctrl Pts',(155.073320605181,4.28224969294531,332.577119389306));
#50623=CARTESIAN_POINT('Ctrl Pts',(155.065571914623,4.21137172848278,332.459619865643));
#50624=CARTESIAN_POINT('Ctrl Pts',(155.057824836245,4.14050851077275,332.342144788737));
#50625=CARTESIAN_POINT('Ctrl Pts',(155.050077757868,4.06470819481683,332.227607226004));
#50626=CARTESIAN_POINT('Ctrl Pts',(155.04233067949,3.98425208980506,332.116439987206));
#50627=CARTESIAN_POINT('Ctrl Pts',(155.034583536184,3.90379531049366,332.00527181672));
#50628=CARTESIAN_POINT('Ctrl Pts',(155.026836392878,3.81868289346691,331.897474343153));
#50629=CARTESIAN_POINT('Ctrl Pts',(155.019089249572,3.7292383710957,331.793449792371));
#50630=CARTESIAN_POINT('Ctrl Pts',(155.011340364544,3.63977373969698,331.689401854661));
#50631=CARTESIAN_POINT('Ctrl Pts',(155.003591479516,3.545975319692,331.589128823943));
#50632=CARTESIAN_POINT('Ctrl Pts',(154.995842594488,3.44820538767936,331.492998051486));
#50633=CARTESIAN_POINT('Ctrl Pts',(154.988085484713,3.35033168165064,331.396765244834));
#50634=CARTESIAN_POINT('Ctrl Pts',(154.980328374939,3.24847832210616,331.304683753611));
#50635=CARTESIAN_POINT('Ctrl Pts',(154.972571265164,3.14304315420253,331.21708276679));
#50636=CARTESIAN_POINT('Ctrl Pts',(154.964810010238,3.03755164511636,331.129434968802));
#50637=CARTESIAN_POINT('Ctrl Pts',(154.957048755311,2.92847482452496,331.04627268282));
#50638=CARTESIAN_POINT('Ctrl Pts',(154.949287500385,2.81624094712037,330.967882691406));
#50639=CARTESIAN_POINT('Ctrl Pts',(154.941513829981,2.70382753208889,330.889367301553));
#50640=CARTESIAN_POINT('Ctrl Pts',(154.933740159576,2.58824729803582,330.815639671812));
#50641=CARTESIAN_POINT('Ctrl Pts',(154.925966489171,2.4699553700999,330.746941861176));
#50642=CARTESIAN_POINT('Ctrl Pts',(154.918554684994,2.35716995986872,330.681441950153));
#50643=CARTESIAN_POINT('Ctrl Pts',(154.911142880817,2.2419198874598,330.620514254845));
#50644=CARTESIAN_POINT('Ctrl Pts',(154.90373107664,2.12461611918627,330.564327626098));
#50645=CARTESIAN_POINT('Ctrl Pts',(154.895955997862,2.00156294379977,330.505387123305));
#50646=CARTESIAN_POINT('Ctrl Pts',(154.888180919083,1.87586079601021,330.451477922936));
#50647=CARTESIAN_POINT('Ctrl Pts',(154.880405840305,1.74795953904585,330.402846477182));
#50648=CARTESIAN_POINT('Ctrl Pts',(154.872640329256,1.62021567272075,330.354274875518));
#50649=CARTESIAN_POINT('Ctrl Pts',(154.864874818207,1.49027844353389,330.310968243642));
#50650=CARTESIAN_POINT('Ctrl Pts',(154.857109307158,1.3586212902708,330.273126693879));
#50651=CARTESIAN_POINT('Ctrl Pts',(154.849351495635,1.2270946754585,330.235322664122));
#50652=CARTESIAN_POINT('Ctrl Pts',(154.841593684113,1.09385190347758,330.202973040348));
#50653=CARTESIAN_POINT('Ctrl Pts',(154.833835872591,0.959384994073779,330.176229328042));
#50654=CARTESIAN_POINT('Ctrl Pts',(154.826083899068,0.825019275283447,330.149505741227));
#50655=CARTESIAN_POINT('Ctrl Pts',(154.818331925545,0.689431634500228,330.128379744851));
#50656=CARTESIAN_POINT('Ctrl Pts',(154.810579952022,0.55312746266412,330.112952519921));
#50657=CARTESIAN_POINT('Ctrl Pts',(154.802831261464,0.416881015725803,330.09753182843));
#50658=CARTESIAN_POINT('Ctrl Pts',(154.795082570907,0.279919028864083,330.087805152105));
#50659=CARTESIAN_POINT('Ctrl Pts',(154.787333880349,0.14275503912601,330.083822210161));
#50660=CARTESIAN_POINT('Ctrl Pts',(154.779586801971,0.00561958750164102,
330.079840096902));
#50661=CARTESIAN_POINT('Ctrl Pts',(154.771839723593,-0.131717392937347,
330.081599352359));
#50662=CARTESIAN_POINT('Ctrl Pts',(154.764092645216,-0.268739710683866,
330.089097635831));
#50663=CARTESIAN_POINT('Ctrl Pts',(154.75634550191,-0.405763176809338,330.096595982145));
#50664=CARTESIAN_POINT('Ctrl Pts',(154.748598358604,-0.542471584691953,
330.109833431053));
#50665=CARTESIAN_POINT('Ctrl Pts',(154.740851215298,-0.678351612092352,
330.128755584774));
#50666=CARTESIAN_POINT('Ctrl Pts',(154.73310233027,-0.814262188207657,330.147681992597));
#50667=CARTESIAN_POINT('Ctrl Pts',(154.725353445242,-0.949343626185989,
330.172295594494));
#50668=CARTESIAN_POINT('Ctrl Pts',(154.717604560214,-1.08309096385484,330.202490539195));
#50669=CARTESIAN_POINT('Ctrl Pts',(154.709847450439,-1.2169802623299,330.232717533121));
#50670=CARTESIAN_POINT('Ctrl Pts',(154.702090340664,-1.34953224996625,330.268537617573));
#50671=CARTESIAN_POINT('Ctrl Pts',(154.69433323089,-1.48025480789057,330.309794379111));
#50672=CARTESIAN_POINT('Ctrl Pts',(154.686571975963,-1.61104721977016,330.351073186944));
#50673=CARTESIAN_POINT('Ctrl Pts',(154.678810721037,-1.74000788669075,330.397794327635));
#50674=CARTESIAN_POINT('Ctrl Pts',(154.671049466111,-1.86666389389016,330.449752867179));
#50675=CARTESIAN_POINT('Ctrl Pts',(154.663275795706,-1.99352250942387,330.501794523452));
#50676=CARTESIAN_POINT('Ctrl Pts',(154.655502125302,-2.11806874282148,330.559090157121));
#50677=CARTESIAN_POINT('Ctrl Pts',(154.647728454897,-2.23985274718433,330.621388035755));
#50678=CARTESIAN_POINT('Ctrl Pts',(154.64031665072,-2.35596767684372,330.68078593315));
#50679=CARTESIAN_POINT('Ctrl Pts',(154.632904846543,-2.4695715028908,330.744730705829));
#50680=CARTESIAN_POINT('Ctrl Pts',(154.625493042366,-2.580299837594,330.812968138333));
#50681=CARTESIAN_POINT('Ctrl Pts',(154.617717963588,-2.69645529782462,330.884550090673));
#50682=CARTESIAN_POINT('Ctrl Pts',(154.609942884809,-2.80981333947447,330.961082346858));
#50683=CARTESIAN_POINT('Ctrl Pts',(154.602167806031,-2.9199232688313,331.042319976724));
#50684=CARTESIAN_POINT('Ctrl Pts',(154.594402294982,-3.02989770091011,331.123457638515));
#50685=CARTESIAN_POINT('Ctrl Pts',(154.586636783933,-3.13663166207078,331.209288923185));
#50686=CARTESIAN_POINT('Ctrl Pts',(154.578871272884,-3.23970066869759,331.299523998221));
#50687=CARTESIAN_POINT('Ctrl Pts',(154.571113461361,-3.34266748210444,331.389669604918));
#50688=CARTESIAN_POINT('Ctrl Pts',(154.563355649839,-3.4419762802728,331.484210056842));
#50689=CARTESIAN_POINT('Ctrl Pts',(154.555597838317,-3.53723339889134,331.582813592403));
#50690=CARTESIAN_POINT('Ctrl Pts',(154.547845864794,-3.63241883350704,331.681342925676));
#50691=CARTESIAN_POINT('Ctrl Pts',(154.540093891271,-3.72355838700805,331.783928976597));
#50692=CARTESIAN_POINT('Ctrl Pts',(154.532341917748,-3.81029347808917,331.890201505993));
#50693=CARTESIAN_POINT('Ctrl Pts',(154.52459322719,-3.89699183680783,331.996429028909));
#50694=CARTESIAN_POINT('Ctrl Pts',(154.516844536632,-3.97928919640726,332.106339622941));
#50695=CARTESIAN_POINT('Ctrl Pts',(154.509095846075,-4.05686584257545,332.21952834975));
#50696=CARTESIAN_POINT('Ctrl Pts',(154.501348767697,-4.13442634827447,332.332693526699));
#50697=CARTESIAN_POINT('Ctrl Pts',(154.493601689319,-4.20726787333821,332.44913515758));
#50698=CARTESIAN_POINT('Ctrl Pts',(154.485854610941,-4.27511304526961,332.568417899255));
#50699=CARTESIAN_POINT('Ctrl Pts',(154.478107467635,-4.34295878580881,332.687701640633));
#50700=CARTESIAN_POINT('Ctrl Pts',(154.47036032433,-4.40580789644616,332.809826200536));
#50701=CARTESIAN_POINT('Ctrl Pts',(154.462613181024,-4.46342833331626,332.934330477581));
#50702=CARTESIAN_POINT('Ctrl Pts',(154.454864295996,-4.52106172448401,333.058862745832));
#50703=CARTESIAN_POINT('Ctrl Pts',(154.447115410968,-4.57346393860177,333.185775441179));
#50704=CARTESIAN_POINT('Ctrl Pts',(154.439366525939,-4.6204507242556,333.314586647963));
#50705=CARTESIAN_POINT('Ctrl Pts',(154.431609416165,-4.66748738216915,333.443534576292));
#50706=CARTESIAN_POINT('Ctrl Pts',(154.42385230639,-4.70909699530752,333.57438467362));
#50707=CARTESIAN_POINT('Ctrl Pts',(154.416095196615,-4.74514478130707,333.706638462403));
#50708=CARTESIAN_POINT('Ctrl Pts',(154.408333941689,-4.78121183009083,333.838962923382));
#50709=CARTESIAN_POINT('Ctrl Pts',(154.400572686763,-4.81171104276371,333.972692189538));
#50710=CARTESIAN_POINT('Ctrl Pts',(154.392811431837,-4.83655883139046,334.107317675206));
#50711=CARTESIAN_POINT('Ctrl Pts',(154.385037761432,-4.86144636838115,334.242158517778));
#50712=CARTESIAN_POINT('Ctrl Pts',(154.377264091027,-4.88066436103362,334.37789805752));
#50713=CARTESIAN_POINT('Ctrl Pts',(154.369490420623,-4.89418105854848,334.514021781717));
#50714=CARTESIAN_POINT('Ctrl Pts',(154.362078616445,-4.90706855054207,334.643808913803));
#50715=CARTESIAN_POINT('Ctrl Pts',(154.354666812268,-4.91477357585445,334.773944980405));
#50716=CARTESIAN_POINT('Ctrl Pts',(154.347255008091,-4.91731271857854,334.903985989534));
#50717=CARTESIAN_POINT('Ctrl Pts',(154.34544246423,-4.91793366152942,334.935787292855));
#50718=CARTESIAN_POINT('Ctrl Pts',(154.343629920369,-4.91824610996808,334.96759463941));
#50719=CARTESIAN_POINT('Ctrl Pts',(154.341817376508,-4.91824996390259,334.999404120642));
#50720=CARTESIAN_POINT('',(152.591817376552,-4.91824825560227,334.995857686006));
#50721=CARTESIAN_POINT('Ctrl Pts',(154.341817376458,-4.91824996390269,334.999404121525));
#50722=CARTESIAN_POINT('Ctrl Pts',(154.334068388395,-4.91826644022024,335.135396025298));
#50723=CARTESIAN_POINT('Ctrl Pts',(154.326319400332,-4.91263828350686,335.271609830519));
#50724=CARTESIAN_POINT('Ctrl Pts',(154.31857041227,-4.90133626904523,335.407536305428));
#50725=CARTESIAN_POINT('Ctrl Pts',(154.310830935574,-4.89004812705442,335.543295939632));
#50726=CARTESIAN_POINT('Ctrl Pts',(154.303091458879,-4.8731000147636,335.678768556545));
#50727=CARTESIAN_POINT('Ctrl Pts',(154.295351982184,-4.8505146831706,335.813443526526));
#50728=CARTESIAN_POINT('Ctrl Pts',(154.28762012185,-4.82795157763601,335.947985963861));
#50729=CARTESIAN_POINT('Ctrl Pts',(154.279888261517,-4.79976235608507,336.081731930328));
#50730=CARTESIAN_POINT('Ctrl Pts',(154.272156401184,-4.7660216451968,336.214174921507));
#50731=CARTESIAN_POINT('Ctrl Pts',(154.264430269083,-4.73230593148192,336.346519790851));
#50732=CARTESIAN_POINT('Ctrl Pts',(154.256704136983,-4.69304701083312,336.477563226027));
#50733=CARTESIAN_POINT('Ctrl Pts',(154.248978004882,-4.64837068851767,336.606808328529));
#50734=CARTESIAN_POINT('Ctrl Pts',(154.241254987576,-4.60371237748629,336.736001325796));
#50735=CARTESIAN_POINT('Ctrl Pts',(154.23353197027,-4.55364113610734,336.863397060586));
#50736=CARTESIAN_POINT('Ctrl Pts',(154.225808952965,-4.49833271458228,336.988513477807));
#50737=CARTESIAN_POINT('Ctrl Pts',(154.218087399298,-4.44303477491628,337.1136061834));
#50738=CARTESIAN_POINT('Ctrl Pts',(154.210365845631,-4.38250178822137,337.236420070549));
#50739=CARTESIAN_POINT('Ctrl Pts',(154.202644291965,-4.31695760137542,337.356493184889));
#50740=CARTESIAN_POINT('Ctrl Pts',(154.194922500902,-4.25141139940418,337.47656999082));
#50741=CARTESIAN_POINT('Ctrl Pts',(154.18720070984,-4.18085387937136,337.593905510588));
#50742=CARTESIAN_POINT('Ctrl Pts',(154.179478918778,-4.10555457456754,337.708062905057));
#50743=CARTESIAN_POINT('Ctrl Pts',(154.171755189466,-4.03023636885367,337.822248954222));
#50744=CARTESIAN_POINT('Ctrl Pts',(154.164031460153,-3.95017422715415,337.93325496234));
#50745=CARTESIAN_POINT('Ctrl Pts',(154.156307730841,-3.86568042395746,338.040673925684));
#50746=CARTESIAN_POINT('Ctrl Pts',(154.148575753182,-3.78109638790026,338.14820760419));
#50747=CARTESIAN_POINT('Ctrl Pts',(154.140843775523,-3.6920714823124,338.252146277603));
#50748=CARTESIAN_POINT('Ctrl Pts',(154.133111797864,-3.59895791905978,338.352116489524));
#50749=CARTESIAN_POINT('Ctrl Pts',(154.125375452798,-3.50579176061177,338.452143169618));
#50750=CARTESIAN_POINT('Ctrl Pts',(154.117639107731,-3.40853262378881,338.548196646541));
#50751=CARTESIAN_POINT('Ctrl Pts',(154.109902762665,-3.30756804918587,338.639941848781));
#50752=CARTESIAN_POINT('Ctrl Pts',(154.102154488962,-3.20644779774817,338.731828512545));
#50753=CARTESIAN_POINT('Ctrl Pts',(154.094406215258,-3.10161099749992,338.819393379673));
#50754=CARTESIAN_POINT('Ctrl Pts',(154.086657941555,-2.99347712926079,338.902342596325));
#50755=CARTESIAN_POINT('Ctrl Pts',(154.080777618976,-2.91141213629057,338.965294444735));
#50756=CARTESIAN_POINT('Ctrl Pts',(154.074897296397,-2.82744881904549,339.02558872054));
#50757=CARTESIAN_POINT('Ctrl Pts',(154.069016973818,-2.74178029713784,339.083114480972));
#50758=CARTESIAN_POINT('Ctrl Pts',(154.06124189504,-2.6285076836539,339.159176178802));
#50759=CARTESIAN_POINT('Ctrl Pts',(154.053466816261,-2.51188855603708,339.230640931774));
#50760=CARTESIAN_POINT('Ctrl Pts',(154.045691737483,-2.39233255663554,339.297200018729));
#50761=CARTESIAN_POINT('Ctrl Pts',(154.037926226434,-2.27292367850251,339.36367720049));
#50762=CARTESIAN_POINT('Ctrl Pts',(154.030160715385,-2.15058545767587,339.425260539293));
#50763=CARTESIAN_POINT('Ctrl Pts',(154.022395204336,-2.02575754522527,339.481683771805));
#50764=CARTESIAN_POINT('Ctrl Pts',(154.014637392813,-1.90105340001345,339.538051060518));
#50765=CARTESIAN_POINT('Ctrl Pts',(154.006879581291,-1.77386482958897,339.589268264628));
#50766=CARTESIAN_POINT('Ctrl Pts',(153.999121769769,-1.6446568780592,339.635114541837));
#50767=CARTESIAN_POINT('Ctrl Pts',(153.991369796246,-1.5155461596102,339.68092631827));
#50768=CARTESIAN_POINT('Ctrl Pts',(153.983617822723,-1.38441945173065,339.721375082611));
#50769=CARTESIAN_POINT('Ctrl Pts',(153.9758658492,-1.25176228377991,339.756287864228));
#50770=CARTESIAN_POINT('Ctrl Pts',(153.968117158642,-1.11916129621872,339.791185860262));
#50771=CARTESIAN_POINT('Ctrl Pts',(153.960368468085,-0.985031514928295,
339.820552437326));
#50772=CARTESIAN_POINT('Ctrl Pts',(153.952619777527,-0.849873947926188,
339.844264375025));
#50773=CARTESIAN_POINT('Ctrl Pts',(153.944872699149,-0.714744501584777,
339.867971379258));
#50774=CARTESIAN_POINT('Ctrl Pts',(153.937125620771,-0.578588079625996,
339.886026016757));
#50775=CARTESIAN_POINT('Ctrl Pts',(153.929378542394,-0.441915820637612,
339.898356200806));
#50776=CARTESIAN_POINT('Ctrl Pts',(153.921631399088,-0.305242416204129,
339.910686488192));
#50777=CARTESIAN_POINT('Ctrl Pts',(153.913884255782,-0.168053555411324,
339.917292191314));
#50778=CARTESIAN_POINT('Ctrl Pts',(153.906137112476,-0.0308650409611062,
339.918153150497));
#50779=CARTESIAN_POINT('Ctrl Pts',(153.898388227448,0.106354316379358,339.919014303242));
#50780=CARTESIAN_POINT('Ctrl Pts',(153.89063934242,0.243572936432081,339.914128139574));
#50781=CARTESIAN_POINT('Ctrl Pts',(153.882890457392,0.380275872842287,339.903526621018));
#50782=CARTESIAN_POINT('Ctrl Pts',(153.875133347617,0.517123907162001,339.892913849901));
#50783=CARTESIAN_POINT('Ctrl Pts',(153.867376237842,0.653454774132652,339.876573636088));
#50784=CARTESIAN_POINT('Ctrl Pts',(153.859619128068,0.788758948637311,339.854589826488));
#50785=CARTESIAN_POINT('Ctrl Pts',(153.851857873142,0.924135425366752,339.832594269444));
#50786=CARTESIAN_POINT('Ctrl Pts',(153.844096618215,1.05848373377354,339.804949186186));
#50787=CARTESIAN_POINT('Ctrl Pts',(153.836335363289,1.19130635864043,339.771789205567));
#50788=CARTESIAN_POINT('Ctrl Pts',(153.828561692885,1.32434145642022,339.738576179785));
#50789=CARTESIAN_POINT('Ctrl Pts',(153.82078802248,1.45584561848945,339.699830738125));
#50790=CARTESIAN_POINT('Ctrl Pts',(153.813014352075,1.58533741116339,339.655737144134));
#50791=CARTESIAN_POINT('Ctrl Pts',(153.805602547898,1.70880132973379,339.613696117551));
#50792=CARTESIAN_POINT('Ctrl Pts',(153.798190743721,1.83043574574425,339.566793749941));
#50793=CARTESIAN_POINT('Ctrl Pts',(153.790778939544,1.94984343437416,339.515229079895));
#50794=CARTESIAN_POINT('Ctrl Pts',(153.783003860766,2.07510364952152,339.461137071766));
#50795=CARTESIAN_POINT('Ctrl Pts',(153.775228781987,2.1983091864865,339.401743237873));
#50796=CARTESIAN_POINT('Ctrl Pts',(153.767453703209,2.31897875408065,339.337224988472));
#50797=CARTESIAN_POINT('Ctrl Pts',(153.75968819216,2.43949983008958,339.272786132884));
#50798=CARTESIAN_POINT('Ctrl Pts',(153.751922681111,2.55749080456709,339.203235591297));
#50799=CARTESIAN_POINT('Ctrl Pts',(153.744157170062,2.67248985057416,339.128798985308));
#50800=CARTESIAN_POINT('Ctrl Pts',(153.736399358539,2.78737487469266,339.054436183429));
#50801=CARTESIAN_POINT('Ctrl Pts',(153.728641547017,2.89927354783543,338.975197169097));
#50802=CARTESIAN_POINT('Ctrl Pts',(153.720883735495,3.00774849695214,338.891353497381));
#50803=CARTESIAN_POINT('Ctrl Pts',(153.713131761972,3.1161418152293,338.807572920688));
#50804=CARTESIAN_POINT('Ctrl Pts',(153.705379788449,3.22111622978268,338.719194821902));
#50805=CARTESIAN_POINT('Ctrl Pts',(153.697627814926,3.32226353812097,338.626533888684));
#50806=CARTESIAN_POINT('Ctrl Pts',(153.689879124368,3.42336801051429,338.533912197426));
#50807=CARTESIAN_POINT('Ctrl Pts',(153.682130433811,3.52064831269694,338.437011542709));
#50808=CARTESIAN_POINT('Ctrl Pts',(153.674381743253,3.61372970182485,338.336186551236));
#50809=CARTESIAN_POINT('Ctrl Pts',(153.666634664875,3.7067917245923,338.235382537245));
#50810=CARTESIAN_POINT('Ctrl Pts',(153.658887586498,3.79565630702035,338.130656097576));
#50811=CARTESIAN_POINT('Ctrl Pts',(153.65114050812,3.87998622343059,338.022398049313));
#50812=CARTESIAN_POINT('Ctrl Pts',(153.643393364814,3.96431684660665,337.914139093742));
#50813=CARTESIAN_POINT('Ctrl Pts',(153.635646221508,4.04411248775849,337.8023487789));
#50814=CARTESIAN_POINT('Ctrl Pts',(153.627899078202,4.11907706374747,337.687449944726));
#50815=CARTESIAN_POINT('Ctrl Pts',(153.620150193174,4.19405849336467,337.572525278855));
#50816=CARTESIAN_POINT('Ctrl Pts',(153.612401308146,4.26420648300821,337.454491030293));
#50817=CARTESIAN_POINT('Ctrl Pts',(153.604652423118,4.32926924278541,337.333797524631));
#50818=CARTESIAN_POINT('Ctrl Pts',(153.596895313343,4.3944010608481,337.212975913634));
#50819=CARTESIAN_POINT('Ctrl Pts',(153.589138203569,4.45443668123103,337.089489751812));
#50820=CARTESIAN_POINT('Ctrl Pts',(153.581381093794,4.50917087931133,336.963812884078));
#50821=CARTESIAN_POINT('Ctrl Pts',(153.573619838868,4.56393432559713,336.838068858644));
#50822=CARTESIAN_POINT('Ctrl Pts',(153.565858583941,4.61339056388664,336.710132159084));
#50823=CARTESIAN_POINT('Ctrl Pts',(153.558097329015,4.65738357242302,336.580494011955));
#50824=CARTESIAN_POINT('Ctrl Pts',(153.550323658611,4.70144695543568,336.450648486039));
#50825=CARTESIAN_POINT('Ctrl Pts',(153.542549988206,4.74002953474878,336.319096448942));
#50826=CARTESIAN_POINT('Ctrl Pts',(153.534776317801,4.77302573011917,336.186342464097));
#50827=CARTESIAN_POINT('Ctrl Pts',(153.527364513624,4.80448594465675,336.059768209186));
#50828=CARTESIAN_POINT('Ctrl Pts',(153.519952709447,4.83086810500045,335.932101671434));
#50829=CARTESIAN_POINT('Ctrl Pts',(153.51254090527,4.85212462580396,335.803784596871));
#50830=CARTESIAN_POINT('Ctrl Pts',(153.504765826492,4.87442299201189,335.669178320247));
#50831=CARTESIAN_POINT('Ctrl Pts',(153.496990747713,4.89115103556317,335.533430744201));
#50832=CARTESIAN_POINT('Ctrl Pts',(153.489215668935,4.90219749024882,335.397042603631));
#50833=CARTESIAN_POINT('Ctrl Pts',(153.481450157886,4.91323035156871,335.260822297352));
#50834=CARTESIAN_POINT('Ctrl Pts',(153.473684646837,4.91859550396333,335.123963380825));
#50835=CARTESIAN_POINT('Ctrl Pts',(153.465919135788,4.91823275638964,334.986976310968));
#50836=CARTESIAN_POINT('Ctrl Pts',(153.458161324266,4.91787036848122,334.85012506419));
#50837=CARTESIAN_POINT('Ctrl Pts',(153.450403512743,4.91179138362069,334.713146305302));
#50838=CARTESIAN_POINT('Ctrl Pts',(153.442645701221,4.89998747060739,334.576554784664));
#50839=CARTESIAN_POINT('Ctrl Pts',(153.434893727698,4.888192440413,334.440066053478));
#50840=CARTESIAN_POINT('Ctrl Pts',(153.427141754175,4.87068109082493,334.303964368362));
#50841=CARTESIAN_POINT('Ctrl Pts',(153.419389780652,4.84749714762111,334.168763291051));
#50842=CARTESIAN_POINT('Ctrl Pts',(153.411641090095,4.82432302283088,334.033619471474));
#50843=CARTESIAN_POINT('Ctrl Pts',(153.403892399537,4.79548114844775,333.899375885559));
#50844=CARTESIAN_POINT('Ctrl Pts',(153.396143708979,4.76106694277791,333.766539571414));
#50845=CARTESIAN_POINT('Ctrl Pts',(153.388396630602,4.72665989727107,333.633730894974));
#50846=CARTESIAN_POINT('Ctrl Pts',(153.380649552224,4.68668292451343,333.502329286061));
#50847=CARTESIAN_POINT('Ctrl Pts',(153.372902473846,4.64128217876355,333.372829818491));
#50848=CARTESIAN_POINT('Ctrl Pts',(153.36515533054,4.59588105251152,333.24332926559));
#50849=CARTESIAN_POINT('Ctrl Pts',(153.357408187234,4.54505619191907,333.115731254692));
#50850=CARTESIAN_POINT('Ctrl Pts',(153.349661043928,4.48900294453701,332.990513591378));
#50851=CARTESIAN_POINT('Ctrl Pts',(153.3419121589,4.43293709519505,332.865267776475));
#50852=CARTESIAN_POINT('Ctrl Pts',(153.334163273872,4.37164067971588,332.742403730741));
#50853=CARTESIAN_POINT('Ctrl Pts',(153.326414388844,4.30535612853699,332.622376886685));
#50854=CARTESIAN_POINT('Ctrl Pts',(153.318657279069,4.23900122225063,332.502222644897));
#50855=CARTESIAN_POINT('Ctrl Pts',(153.310900169295,4.16764779334477,332.384911963116));
#50856=CARTESIAN_POINT('Ctrl Pts',(153.30314305952,4.09158324929788,332.27087384378));
#50857=CARTESIAN_POINT('Ctrl Pts',(153.295381804594,4.01547805879082,332.156774786119));
#50858=CARTESIAN_POINT('Ctrl Pts',(153.287620549668,3.93465696705778,332.0459520911));
#50859=CARTESIAN_POINT('Ctrl Pts',(153.279859294741,3.84944862466571,331.938802791626));
#50860=CARTESIAN_POINT('Ctrl Pts',(153.272085624337,3.76410397669504,331.831482088191));
#50861=CARTESIAN_POINT('Ctrl Pts',(153.264311953932,3.67435830969433,331.727846818396));
#50862=CARTESIAN_POINT('Ctrl Pts',(153.256538283527,3.58057878629284,331.628258815145));
#50863=CARTESIAN_POINT('Ctrl Pts',(153.24912647935,3.49116472226735,331.533306657404));
#50864=CARTESIAN_POINT('Ctrl Pts',(153.241714675173,3.39808410779581,331.44203364685));
#50865=CARTESIAN_POINT('Ctrl Pts',(153.234302870996,3.3016826653762,331.35471885314));
#50866=CARTESIAN_POINT('Ctrl Pts',(153.226527792218,3.20055630109902,331.263124501293));
#50867=CARTESIAN_POINT('Ctrl Pts',(153.218752713439,3.0954557725751,331.175596730001));
#50868=CARTESIAN_POINT('Ctrl Pts',(153.210977634661,2.98674194593264,331.092500081778));
#50869=CARTESIAN_POINT('Ctrl Pts',(153.203212123612,2.87816189857511,331.009505689271));
#50870=CARTESIAN_POINT('Ctrl Pts',(153.195446612563,2.76597770772391,330.930931805466));
#50871=CARTESIAN_POINT('Ctrl Pts',(153.187681101514,2.6505860546638,330.857105283824));
#50872=CARTESIAN_POINT('Ctrl Pts',(153.179923289992,2.53530881276349,330.783351961392));
#50873=CARTESIAN_POINT('Ctrl Pts',(153.172165478469,2.41683076458076,330.714336843177));
#50874=CARTESIAN_POINT('Ctrl Pts',(153.164407666947,2.29558026618454,330.650345496019));
#50875=CARTESIAN_POINT('Ctrl Pts',(153.156655693424,2.1744210126331,330.586402304378));
#50876=CARTESIAN_POINT('Ctrl Pts',(153.148903719901,2.05049380595286,330.527475540505));
#50877=CARTESIAN_POINT('Ctrl Pts',(153.141151746378,1.92425417369,330.473806352183));
#50878=CARTESIAN_POINT('Ctrl Pts',(153.13340305582,1.79806800398664,330.420159892794));
#50879=CARTESIAN_POINT('Ctrl Pts',(153.125654365263,1.6695717154537,330.371766733043));
#50880=CARTESIAN_POINT('Ctrl Pts',(153.117905674705,1.53924332357645,330.328821021056));
#50881=CARTESIAN_POINT('Ctrl Pts',(153.110158596327,1.40894204760965,330.285884244283));
#50882=CARTESIAN_POINT('Ctrl Pts',(153.10241151795,1.2768097975067,330.248392783141));
#50883=CARTESIAN_POINT('Ctrl Pts',(153.094664439572,1.1433419838573,330.216491646244));
#50884=CARTESIAN_POINT('Ctrl Pts',(153.086917296266,1.00987305161915,330.184590241986));
#50885=CARTESIAN_POINT('Ctrl Pts',(153.07917015296,0.875068913674467,330.158279346289));
#50886=CARTESIAN_POINT('Ctrl Pts',(153.071423009654,0.739437080699412,330.137653255249));
#50887=CARTESIAN_POINT('Ctrl Pts',(153.063674124626,0.603774754808598,330.117022527026));
#50888=CARTESIAN_POINT('Ctrl Pts',(153.055925239598,0.467284749958108,330.10207920542));
#50889=CARTESIAN_POINT('Ctrl Pts',(153.04817635457,0.330481242081419,330.092865886168));
#50890=CARTESIAN_POINT('Ctrl Pts',(153.040419244795,0.193532529548,330.083642787804));
#50891=CARTESIAN_POINT('Ctrl Pts',(153.032662135021,0.0562700398851874,
330.080161867232));
#50892=CARTESIAN_POINT('Ctrl Pts',(153.024905025246,-0.0807899369280585,
330.082413595208));
#50893=CARTESIAN_POINT('Ctrl Pts',(153.01714377032,-0.217923154210515,330.084666526436));
#50894=CARTESIAN_POINT('Ctrl Pts',(153.009382515393,-0.354853253000151,
330.092658187437));
#50895=CARTESIAN_POINT('Ctrl Pts',(153.001621260467,-0.491068508180668,
330.106327066224));
#50896=CARTESIAN_POINT('Ctrl Pts',(152.993847590063,-0.627501663376957,
330.120017810762));
#50897=CARTESIAN_POINT('Ctrl Pts',(152.986073919658,-0.763217302728808,
330.139403865706));
#50898=CARTESIAN_POINT('Ctrl Pts',(152.978300249253,-0.897712460460137,
330.164372284715));
#50899=CARTESIAN_POINT('Ctrl Pts',(152.970888445076,-1.02594683624091,330.188178417812));
#50900=CARTESIAN_POINT('Ctrl Pts',(152.963476640899,-1.15307151949375,330.217058829054));
#50901=CARTESIAN_POINT('Ctrl Pts',(152.956064836722,-1.27866474430995,330.25087381362));
#50902=CARTESIAN_POINT('Ctrl Pts',(152.948289757944,-1.41041366719782,330.28634617131));
#50903=CARTESIAN_POINT('Ctrl Pts',(152.940514679165,-1.54089356405185,330.327361148579));
#50904=CARTESIAN_POINT('Ctrl Pts',(152.932739600387,-1.66960259792616,330.373812560272));
#50905=CARTESIAN_POINT('Ctrl Pts',(152.924974089338,-1.79815324714006,330.420206810546));
#50906=CARTESIAN_POINT('Ctrl Pts',(152.917208578289,-1.92493700512896,330.472024052882));
#50907=CARTESIAN_POINT('Ctrl Pts',(152.90944306724,-2.04946434684033,330.529107588688));
#50908=CARTESIAN_POINT('Ctrl Pts',(152.901685255718,-2.17386821932953,330.586134526001));
#50909=CARTESIAN_POINT('Ctrl Pts',(152.893927444195,-2.29601977474991,330.648417203783));
#50910=CARTESIAN_POINT('Ctrl Pts',(152.886169632673,-2.4154470658049,330.71574994488));
#50911=CARTESIAN_POINT('Ctrl Pts',(152.87841765915,-2.53478448403676,330.783032015955));
#50912=CARTESIAN_POINT('Ctrl Pts',(152.870665685627,-2.65140137940108,330.855356394774));
#50913=CARTESIAN_POINT('Ctrl Pts',(152.862913712104,-2.76484845348901,330.93247051741));
#50914=CARTESIAN_POINT('Ctrl Pts',(152.855165021547,-2.87824748267329,331.009551982169));
#50915=CARTESIAN_POINT('Ctrl Pts',(152.847416330989,-2.98847903797123,331.091418937004));
#50916=CARTESIAN_POINT('Ctrl Pts',(152.839667640431,-3.09512117447386,331.177774473187));
#50917=CARTESIAN_POINT('Ctrl Pts',(152.831920562054,-3.20174112318953,331.264112042379));
#50918=CARTESIAN_POINT('Ctrl Pts',(152.824173483676,-3.30477283498708,331.354936089525));
#50919=CARTESIAN_POINT('Ctrl Pts',(152.816426405298,-3.4038262739316,331.449908485772));
#50920=CARTESIAN_POINT('Ctrl Pts',(152.808679261992,-3.50288054303916,331.544881677979));
#50921=CARTESIAN_POINT('Ctrl Pts',(152.800932118686,-3.59795619065016,331.644003018117));
#50922=CARTESIAN_POINT('Ctrl Pts',(152.793184975381,-3.68869927801971,331.746896758657));
#50923=CARTESIAN_POINT('Ctrl Pts',(152.785436090353,-3.77946276636137,331.849813631894));
#50924=CARTESIAN_POINT('Ctrl Pts',(152.777687205324,-3.86589149772046,331.95650430009));
#50925=CARTESIAN_POINT('Ctrl Pts',(152.769938320296,-3.94767140233244,332.06655943273));
#50926=CARTESIAN_POINT('Ctrl Pts',(152.762181210522,-4.0295381089806,332.176731379025));
#50927=CARTESIAN_POINT('Ctrl Pts',(152.754424100747,-4.10674589862775,332.290274609093));
#50928=CARTESIAN_POINT('Ctrl Pts',(152.746666990972,-4.17902339048772,332.406749806853));
#50929=CARTESIAN_POINT('Ctrl Pts',(152.738905736046,-4.2513395051283,332.523287245235));
#50930=CARTESIAN_POINT('Ctrl Pts',(152.73114448112,-4.31871988040013,332.642759432912));
#50931=CARTESIAN_POINT('Ctrl Pts',(152.723383226194,-4.38093931922371,332.764702761649));
#50932=CARTESIAN_POINT('Ctrl Pts',(152.715609555789,-4.44325828887223,332.886841159971));
#50933=CARTESIAN_POINT('Ctrl Pts',(152.707835885384,-4.50039966150176,333.01145824317));
#50934=CARTESIAN_POINT('Ctrl Pts',(152.70006221498,-4.55218623245835,333.138069934848));
#50935=CARTESIAN_POINT('Ctrl Pts',(152.692650410803,-4.60156212607905,333.25878782182));
#50936=CARTESIAN_POINT('Ctrl Pts',(152.685238606625,-4.64607043265146,333.381318527738));
#50937=CARTESIAN_POINT('Ctrl Pts',(152.677826802448,-4.6856003912053,333.505231778356));
#50938=CARTESIAN_POINT('Ctrl Pts',(152.66845128616,-4.73560357011186,333.661975085615));
#50939=CARTESIAN_POINT('Ctrl Pts',(152.659075769872,-4.77777038081238,333.821331555862));
#50940=CARTESIAN_POINT('Ctrl Pts',(152.649700253583,-4.8118660837572,333.982587667419));
#50941=CARTESIAN_POINT('Ctrl Pts',(152.640053107411,-4.84694961622879,334.14851573276));
#50942=CARTESIAN_POINT('Ctrl Pts',(152.63040596124,-4.87348721353554,334.316455231313));
#50943=CARTESIAN_POINT('Ctrl Pts',(152.620758815068,-4.89127597027851,334.485604777359));
#50944=CARTESIAN_POINT('Ctrl Pts',(152.611111668896,-4.90906472702148,334.654754323405));
#50945=CARTESIAN_POINT('Ctrl Pts',(152.601464522724,-4.91810444946375,334.82511392033));
#50946=CARTESIAN_POINT('Ctrl Pts',(152.591817376552,-4.91824825560227,334.995857686006));
#50947=CARTESIAN_POINT('',(150.841817376458,-4.91824934725888,335.002533907583));
#50948=CARTESIAN_POINT('Ctrl Pts',(152.591817376508,-4.91824825560293,334.995857686791));
#50949=CARTESIAN_POINT('Ctrl Pts',(152.583807851161,-4.91836765036206,335.137617383878));
#50950=CARTESIAN_POINT('Ctrl Pts',(152.575798325814,-4.91235312101776,335.279476192963));
#50951=CARTESIAN_POINT('Ctrl Pts',(152.567788800466,-4.90021012118859,335.420860821057));
#50952=CARTESIAN_POINT('Ctrl Pts',(152.560077369643,-4.88851905347684,335.556983466507));
#50953=CARTESIAN_POINT('Ctrl Pts',(152.552365938819,-4.87114755500484,335.692666168221));
#50954=CARTESIAN_POINT('Ctrl Pts',(152.544654507995,-4.84815353813783,335.827399742048));
#50955=CARTESIAN_POINT('Ctrl Pts',(152.536943499239,-4.8251607797939,335.962125941552));
#50956=CARTESIAN_POINT('Ctrl Pts',(152.529232490482,-4.79654618123677,336.095902727458));
#50957=CARTESIAN_POINT('Ctrl Pts',(152.521521481725,-4.76241910271695,336.228229356666));
#50958=CARTESIAN_POINT('Ctrl Pts',(152.513809188586,-4.72828633982835,336.360578026829));
#50959=CARTESIAN_POINT('Ctrl Pts',(152.506096895447,-4.68863936876036,336.491475677609));
#50960=CARTESIAN_POINT('Ctrl Pts',(152.498384602308,-4.64363779901445,336.620435451989));
#50961=CARTESIAN_POINT('Ctrl Pts',(152.490669317794,-4.59861877446086,336.749445246138));
#50962=CARTESIAN_POINT('Ctrl Pts',(152.482954033279,-4.54824114900427,336.876515296162));
#50963=CARTESIAN_POINT('Ctrl Pts',(152.475238748765,-4.49271299228432,337.001177910996));
#50964=CARTESIAN_POINT('Ctrl Pts',(152.467514516525,-4.43712043733058,337.125985102072));
#50965=CARTESIAN_POINT('Ctrl Pts',(152.459790284285,-4.37636558809715,337.248378924183));
#50966=CARTESIAN_POINT('Ctrl Pts',(152.452066052045,-4.31070304883258,337.367915177384));
#50967=CARTESIAN_POINT('Ctrl Pts',(152.444336503922,-4.24499532004474,337.487533696461));
#50968=CARTESIAN_POINT('Ctrl Pts',(152.436606955799,-4.17437337887094,337.604290393913));
#50969=CARTESIAN_POINT('Ctrl Pts',(152.428877407677,-4.0991349989026,337.717770285229));
#50970=CARTESIAN_POINT('Ctrl Pts',(152.421136704814,-4.02378804020096,337.831413942735));
#50971=CARTESIAN_POINT('Ctrl Pts',(152.413396001951,-3.94381157655401,337.941771038094));
#50972=CARTESIAN_POINT('Ctrl Pts',(152.405655299089,-3.85954365291573,338.048459587027));
#50973=CARTESIAN_POINT('Ctrl Pts',(152.403633122117,-3.83752954674917,338.076330845052));
#50974=CARTESIAN_POINT('Ctrl Pts',(152.401610945146,-3.81522275940396,338.1039519362));
#50975=CARTESIAN_POINT('Ctrl Pts',(152.399588768174,-3.79262971843772,338.13131647735));
#50976=CARTESIAN_POINT('Ctrl Pts',(152.391813689396,-3.7057616174606,338.236530544255));
#50977=CARTESIAN_POINT('Ctrl Pts',(152.384038610617,-3.6143747021492,338.338293325041));
#50978=CARTESIAN_POINT('Ctrl Pts',(152.376263531839,-3.51877352575847,338.436192069271));
#50979=CARTESIAN_POINT('Ctrl Pts',(152.36849802079,-3.42328999270159,338.533970342864));
#50980=CARTESIAN_POINT('Ctrl Pts',(152.360732509741,-3.32360278753055,338.627893763896));
#50981=CARTESIAN_POINT('Ctrl Pts',(152.352966998692,-3.22005733709591,338.717581715082));
#50982=CARTESIAN_POINT('Ctrl Pts',(152.34520918717,-3.11661455227666,338.807180740405));
#50983=CARTESIAN_POINT('Ctrl Pts',(152.337451375648,-3.00932142862713,338.892552398822));
#50984=CARTESIAN_POINT('Ctrl Pts',(152.329693564125,-2.89856068800378,338.973352362988));
#50985=CARTESIAN_POINT('Ctrl Pts',(152.321941590602,-2.78788329835027,339.054091522617));
#50986=CARTESIAN_POINT('Ctrl Pts',(152.314189617079,-2.67374380029645,339.130265606399));
#50987=CARTESIAN_POINT('Ctrl Pts',(152.306437643556,-2.55655820592767,339.201570325748));
#50988=CARTESIAN_POINT('Ctrl Pts',(152.298688952999,-2.43942223972767,339.272844847505));
#50989=CARTESIAN_POINT('Ctrl Pts',(152.290940262441,-2.31924307620051,339.339253903599));
#50990=CARTESIAN_POINT('Ctrl Pts',(152.283191571884,-2.19646575499314,339.400536472936));
#50991=CARTESIAN_POINT('Ctrl Pts',(152.275444493506,-2.07371397863294,339.461806291923));
#50992=CARTESIAN_POINT('Ctrl Pts',(152.267697415128,-1.94836546933115,339.517951571258));
#50993=CARTESIAN_POINT('Ctrl Pts',(152.25995033675,-1.82088956307833,339.568757408921));
#50994=CARTESIAN_POINT('Ctrl Pts',(152.252203193444,-1.69341258845472,339.619563672386));
#50995=CARTESIAN_POINT('Ctrl Pts',(152.244456050138,-1.56380854441616,339.665030260208));
#50996=CARTESIAN_POINT('Ctrl Pts',(152.236708906833,-1.43256605030295,339.704990709238));
#50997=CARTESIAN_POINT('Ctrl Pts',(152.228960021804,-1.30129405009066,339.744960142226));
#50998=CARTESIAN_POINT('Ctrl Pts',(152.221211136776,-1.16838324066433,339.779420859315));
#50999=CARTESIAN_POINT('Ctrl Pts',(152.213462251748,-1.03433628902268,339.808256597116));
#51000=CARTESIAN_POINT('Ctrl Pts',(152.205705141974,-0.900147058561605,
339.837122941467));
#51001=CARTESIAN_POINT('Ctrl Pts',(152.197948032199,-0.764819659696912,
339.860352297742));
#51002=CARTESIAN_POINT('Ctrl Pts',(152.190190922424,-0.628866364604577,
339.877879678505));
#51003=CARTESIAN_POINT('Ctrl Pts',(152.182429667498,-0.492840420418242,
339.895416425339));
#51004=CARTESIAN_POINT('Ctrl Pts',(152.174668412572,-0.356188302785288,
339.907245091643));
#51005=CARTESIAN_POINT('Ctrl Pts',(152.166907157646,-0.219425259392771,
339.913352787867));
#51006=CARTESIAN_POINT('Ctrl Pts',(152.159133487241,-0.0824434397018431,
339.919470254415));
#51007=CARTESIAN_POINT('Ctrl Pts',(152.151359816836,0.0546492692580443,
339.919848462023));
#51008=CARTESIAN_POINT('Ctrl Pts',(152.143586146431,0.191338874009855,339.914526680952));
#51009=CARTESIAN_POINT('Ctrl Pts',(152.136174342254,0.32166554477545,339.909452630071));
#51010=CARTESIAN_POINT('Ctrl Pts',(152.128762538077,0.451625508863558,339.899197339723));
#51011=CARTESIAN_POINT('Ctrl Pts',(152.1213507339,0.580781267816581,339.883838263237));
#51012=CARTESIAN_POINT('Ctrl Pts',(152.113575655122,0.716267335250423,339.86772639266));
#51013=CARTESIAN_POINT('Ctrl Pts',(152.105800576343,0.851296532281904,339.84594686575));
#51014=CARTESIAN_POINT('Ctrl Pts',(152.098025497565,0.985356957022539,339.818532424893));
#51015=CARTESIAN_POINT('Ctrl Pts',(152.090259986516,1.11925241187564,339.791151719251));
#51016=CARTESIAN_POINT('Ctrl Pts',(152.082494475467,1.25218108715821,339.758149974135));
#51017=CARTESIAN_POINT('Ctrl Pts',(152.074728964418,1.38363598338646,339.7196116925));
#51018=CARTESIAN_POINT('Ctrl Pts',(152.066971152896,1.51496054170246,339.681111621683));
#51019=CARTESIAN_POINT('Ctrl Pts',(152.059213341373,1.64481385627521,339.637086048002));
#51020=CARTESIAN_POINT('Ctrl Pts',(152.051455529851,1.77269926213441,339.587670475146));
#51021=CARTESIAN_POINT('Ctrl Pts',(152.043703556328,1.90048843017039,339.538292089076));
#51022=CARTESIAN_POINT('Ctrl Pts',(152.035951582805,2.02631227404551,339.483531917705));
#51023=CARTESIAN_POINT('Ctrl Pts',(152.028199609282,2.14968978298609,339.423575126459));
#51024=CARTESIAN_POINT('Ctrl Pts',(152.020450918724,2.27301504147835,339.363643726949));
#51025=CARTESIAN_POINT('Ctrl Pts',(152.012702228167,2.39389567478669,339.298520255233));
#51026=CARTESIAN_POINT('Ctrl Pts',(152.004953537609,2.51187134821484,339.228437701151));
#51027=CARTESIAN_POINT('Ctrl Pts',(151.997206459231,2.6298224758187,339.158369728331));
#51028=CARTESIAN_POINT('Ctrl Pts',(151.989459380854,2.74486950989806,339.08334492493));
#51029=CARTESIAN_POINT('Ctrl Pts',(151.981712302476,2.85657775012334,339.00364166978));
#51030=CARTESIAN_POINT('Ctrl Pts',(151.97396515917,2.96828692657116,338.923937746641));
#51031=CARTESIAN_POINT('Ctrl Pts',(151.966218015864,3.07665693516562,338.839555520571));
#51032=CARTESIAN_POINT('Ctrl Pts',(151.958470872558,3.1812833735312,338.750815799235));
#51033=CARTESIAN_POINT('Ctrl Pts',(151.95072198753,3.28593333414165,338.662056127327));
#51034=CARTESIAN_POINT('Ctrl Pts',(151.942973102502,3.38683775173035,338.568937263524));
#51035=CARTESIAN_POINT('Ctrl Pts',(151.935224217474,3.48362683597688,338.471818994441));
#51036=CARTESIAN_POINT('Ctrl Pts',(151.927467107699,3.58051865315734,338.374597643024));
#51037=CARTESIAN_POINT('Ctrl Pts',(151.919709997925,3.67328613503527,338.273368683815));
#51038=CARTESIAN_POINT('Ctrl Pts',(151.91195288815,3.761597412422,338.168527728987));
#51039=CARTESIAN_POINT('Ctrl Pts',(151.904191633224,3.84995588053175,338.063630750505));
#51040=CARTESIAN_POINT('Ctrl Pts',(151.896430378297,3.93385316032766,337.955118239508));
#51041=CARTESIAN_POINT('Ctrl Pts',(151.888669123371,4.01299958262628,337.843416503494));
#51042=CARTESIAN_POINT('Ctrl Pts',(151.880895452967,4.0922726134067,337.731536081106));
#51043=CARTESIAN_POINT('Ctrl Pts',(151.873121782562,4.16677938744925,337.616456567235));
#51044=CARTESIAN_POINT('Ctrl Pts',(151.865348112157,4.23627477659072,337.498631441354));
#51045=CARTESIAN_POINT('Ctrl Pts',(151.85793630798,4.30253513864828,337.386291103428));
#51046=CARTESIAN_POINT('Ctrl Pts',(151.850524503803,4.36424003987656,337.271455270997));
#51047=CARTESIAN_POINT('Ctrl Pts',(151.843112699626,4.42121785691321,337.154533760286));
#51048=CARTESIAN_POINT('Ctrl Pts',(151.835337620848,4.48098832649089,337.031881578044));
#51049=CARTESIAN_POINT('Ctrl Pts',(151.827562542069,4.53574550415438,336.906546493819));
#51050=CARTESIAN_POINT('Ctrl Pts',(151.819787463291,4.58523990418909,336.778976695612));
#51051=CARTESIAN_POINT('Ctrl Pts',(151.812021952242,4.63467339821358,336.651563880164));
#51052=CARTESIAN_POINT('Ctrl Pts',(151.804256441193,4.67885686032506,336.521922183288));
#51053=CARTESIAN_POINT('Ctrl Pts',(151.796490930144,4.71758698434946,336.390523681063));
#51054=CARTESIAN_POINT('Ctrl Pts',(151.788733118621,4.75627870734306,336.259255460836));
#51055=CARTESIAN_POINT('Ctrl Pts',(151.780975307099,4.78952774268754,336.126234274207));
#51056=CARTESIAN_POINT('Ctrl Pts',(151.773217495577,4.81717926441125,335.991951106167));
#51057=CARTESIAN_POINT('Ctrl Pts',(151.765465522054,4.84480997748797,335.85776899047));
#51058=CARTESIAN_POINT('Ctrl Pts',(151.757713548531,4.86685148281693,335.722327164955));
#51059=CARTESIAN_POINT('Ctrl Pts',(151.749961575008,4.88319918742346,335.58613032548));
#51060=CARTESIAN_POINT('Ctrl Pts',(151.74221288445,4.8995399687674,335.449991165447));
#51061=CARTESIAN_POINT('Ctrl Pts',(151.734464193893,4.91019169886501,335.313098014693));
#51062=CARTESIAN_POINT('Ctrl Pts',(151.726715503335,4.91510119032694,335.175964062657));
#51063=CARTESIAN_POINT('Ctrl Pts',(151.718968424957,4.92000966032816,335.038858642485));
#51064=CARTESIAN_POINT('Ctrl Pts',(151.71122134658,4.91917825410186,334.901512911064));
#51065=CARTESIAN_POINT('Ctrl Pts',(151.703474268202,4.91260582505575,334.764443063935));
#51066=CARTESIAN_POINT('Ctrl Pts',(151.695727124896,4.90603334092635,334.627372068028));
#51067=CARTESIAN_POINT('Ctrl Pts',(151.68797998159,4.89371975672828,334.490577351451));
#51068=CARTESIAN_POINT('Ctrl Pts',(151.680232838284,4.87571600114181,334.354572592223));
#51069=CARTESIAN_POINT('Ctrl Pts',(151.672483953256,4.85770819792885,334.218537256238));
#51070=CARTESIAN_POINT('Ctrl Pts',(151.664735068228,4.8340077290053,334.083292618424));
#51071=CARTESIAN_POINT('Ctrl Pts',(151.6569861832,4.80471703184798,333.949344344531));
#51072=CARTESIAN_POINT('Ctrl Pts',(151.649229073425,4.77539524524206,333.815253896555));
#51073=CARTESIAN_POINT('Ctrl Pts',(151.641471963651,4.7404714612595,333.682462943592));
#51074=CARTESIAN_POINT('Ctrl Pts',(151.633714853876,4.700098765155,333.551464649969));
#51075=CARTESIAN_POINT('Ctrl Pts',(151.62595359895,4.65970449517258,333.420396355047));
#51076=CARTESIAN_POINT('Ctrl Pts',(151.618192344023,4.61385564178444,333.291122996449));
#51077=CARTESIAN_POINT('Ctrl Pts',(151.610431089097,4.56275393944487,333.164118862622));
#51078=CARTESIAN_POINT('Ctrl Pts',(151.602657418693,4.51157049103557,333.036911563571));
#51079=CARTESIAN_POINT('Ctrl Pts',(151.594883748288,4.45511756334005,332.91198109953));
#51080=CARTESIAN_POINT('Ctrl Pts',(151.587110077883,4.39364384400625,332.789779007763));
#51081=CARTESIAN_POINT('Ctrl Pts',(151.579698273706,4.33503174109739,332.673265452768));
#51082=CARTESIAN_POINT('Ctrl Pts',(151.572286469529,4.27185590237207,332.559232226702));
#51083=CARTESIAN_POINT('Ctrl Pts',(151.564874665352,4.20436807578962,332.448045426388));
#51084=CARTESIAN_POINT('Ctrl Pts',(151.557099586574,4.13357246979034,332.331409029781));
#51085=CARTESIAN_POINT('Ctrl Pts',(151.549324507795,4.05780777435867,332.217536545091));
#51086=CARTESIAN_POINT('Ctrl Pts',(151.541549429017,3.97731586931176,332.106880310423));
#51087=CARTESIAN_POINT('Ctrl Pts',(151.533783917968,3.89692301467819,331.996360245295));
#51088=CARTESIAN_POINT('Ctrl Pts',(151.526018406919,3.81181475258537,331.889048868374));
#51089=CARTESIAN_POINT('Ctrl Pts',(151.51825289587,3.72227804124411,331.785372611612));
#51090=CARTESIAN_POINT('Ctrl Pts',(151.510495084348,3.63283010581321,331.681799150162));
#51091=CARTESIAN_POINT('Ctrl Pts',(151.502737272826,3.53896271294899,331.581853930165));
#51092=CARTESIAN_POINT('Ctrl Pts',(151.494979461303,3.44100495718743,331.485932848235));
#51093=CARTESIAN_POINT('Ctrl Pts',(151.48722748778,3.34312091774286,331.390083949961));
#51094=CARTESIAN_POINT('Ctrl Pts',(151.479475514257,3.24115292041716,331.298253434458));
#51095=CARTESIAN_POINT('Ctrl Pts',(151.471723540734,3.13546877346369,331.210802376078));
#51096=CARTESIAN_POINT('Ctrl Pts',(151.463974850177,3.02982938380956,331.123388353274));
#51097=CARTESIAN_POINT('Ctrl Pts',(151.456226159619,2.9204772752052,331.04035034739));
#51098=CARTESIAN_POINT('Ctrl Pts',(151.448477469062,2.80781521685033,330.962010801089));
#51099=CARTESIAN_POINT('Ctrl Pts',(151.440730390684,2.69517659877782,330.883687553985));
#51100=CARTESIAN_POINT('Ctrl Pts',(151.432983312306,2.57922972146833,330.81006104505));
#51101=CARTESIAN_POINT('Ctrl Pts',(151.425236233928,2.46040804427769,330.741411581503));
#51102=CARTESIAN_POINT('Ctrl Pts',(151.417489090622,2.34158537124667,330.672761542608));
#51103=CARTESIAN_POINT('Ctrl Pts',(151.409741947317,2.21988818872619,330.60908882784));
#51104=CARTESIAN_POINT('Ctrl Pts',(151.401994804011,2.09577601995414,330.550628590836));
#51105=CARTESIAN_POINT('Ctrl Pts',(151.394245918983,1.97163594813191,330.49215521073));
#51106=CARTESIAN_POINT('Ctrl Pts',(151.386497033955,1.84508016320923,330.438896806818));
#51107=CARTESIAN_POINT('Ctrl Pts',(151.378748148927,1.7165893250997,330.391040881994));
#51108=CARTESIAN_POINT('Ctrl Pts',(151.370991039152,1.58796210548695,330.343134162396));
#51109=CARTESIAN_POINT('Ctrl Pts',(151.363233929377,1.45739609673067,330.300641513222));
#51110=CARTESIAN_POINT('Ctrl Pts',(151.355476819602,1.3253888544502,330.26370108133));
#51111=CARTESIAN_POINT('Ctrl Pts',(151.347715564676,1.19331107172027,330.226740909652));
#51112=CARTESIAN_POINT('Ctrl Pts',(151.33995430975,1.05979090117466,330.195338956567));
#51113=CARTESIAN_POINT('Ctrl Pts',(151.332193054824,0.925336352174291,330.169582243962));
#51114=CARTESIAN_POINT('Ctrl Pts',(151.324419384419,0.790666719713976,330.143784329011));
#51115=CARTESIAN_POINT('Ctrl Pts',(151.316645714015,0.655060108782703,330.123649757679));
#51116=CARTESIAN_POINT('Ctrl Pts',(151.30887204361,0.51903080585563,330.109213755941));
#51117=CARTESIAN_POINT('Ctrl Pts',(151.301460239433,0.389333699706613,330.095449753558));
#51118=CARTESIAN_POINT('Ctrl Pts',(151.294048435256,0.259252655752013,330.08686574229));
#51119=CARTESIAN_POINT('Ctrl Pts',(151.286636631079,0.129231767886393,330.083448137905));
#51120=CARTESIAN_POINT('Ctrl Pts',(151.2788615523,-0.00716183100589846,
330.079863026549));
#51121=CARTESIAN_POINT('Ctrl Pts',(151.271086473522,-0.143920256820354,
330.081952239839));
#51122=CARTESIAN_POINT('Ctrl Pts',(151.263311394744,-0.280532233746121,
330.08975716198));
#51123=CARTESIAN_POINT('Ctrl Pts',(151.255545883695,-0.416976100936998,
330.097552479667));
#51124=CARTESIAN_POINT('Ctrl Pts',(151.247780372645,-0.553273491307314,
330.111049489388));
#51125=CARTESIAN_POINT('Ctrl Pts',(151.240014861596,-0.688910519575954,
330.130237648661));
#51126=CARTESIAN_POINT('Ctrl Pts',(151.232257050074,-0.824413063335708,
330.149406782818));
#51127=CARTESIAN_POINT('Ctrl Pts',(151.224499238552,-0.959256163457514,
330.174255782655));
#51128=CARTESIAN_POINT('Ctrl Pts',(151.21674142703,-1.09292881009604,330.204722147929));
#51129=CARTESIAN_POINT('Ctrl Pts',(151.208989453507,-1.22650086382965,330.235165586298));
#51130=CARTESIAN_POINT('Ctrl Pts',(151.201237479984,-1.35890383770935,330.271217889468));
#51131=CARTESIAN_POINT('Ctrl Pts',(151.193485506461,-1.48963505445896,330.312765157683));
#51132=CARTESIAN_POINT('Ctrl Pts',(151.185736815903,-1.6203109064604,330.354294830606));
#51133=CARTESIAN_POINT('Ctrl Pts',(151.177988125346,-1.74931603773501,330.401314721953));
#51134=CARTESIAN_POINT('Ctrl Pts',(151.170239434788,-1.87616133784369,330.453660626737));
#51135=CARTESIAN_POINT('Ctrl Pts',(151.16249235641,-2.00298024672811,330.505995640519));
#51136=CARTESIAN_POINT('Ctrl Pts',(151.154745278032,-2.12763985718702,330.563654314594));
#51137=CARTESIAN_POINT('Ctrl Pts',(151.146998199654,-2.24966988316949,330.626423834062));
#51138=CARTESIAN_POINT('Ctrl Pts',(151.139251056349,-2.37170093188103,330.6891938796));
#51139=CARTESIAN_POINT('Ctrl Pts',(151.131503913043,-2.49110200457205,330.757074677176));
#51140=CARTESIAN_POINT('Ctrl Pts',(151.123756769737,-2.60742668113987,330.829807059022));
#51141=CARTESIAN_POINT('Ctrl Pts',(151.116007884709,-2.72377750996423,330.902555792652));
#51142=CARTESIAN_POINT('Ctrl Pts',(151.108258999681,-2.83705023502251,330.98015807382));
#51143=CARTESIAN_POINT('Ctrl Pts',(151.100510114653,-2.94682706847255,331.062311173922));
#51144=CARTESIAN_POINT('Ctrl Pts',(151.092753004878,-3.05672042018824,331.144551472174));
#51145=CARTESIAN_POINT('Ctrl Pts',(151.084995895103,-3.16311015463384,331.231352003745));
#51146=CARTESIAN_POINT('Ctrl Pts',(151.077238785329,-3.26561084527332,331.322369122691));
#51147=CARTESIAN_POINT('Ctrl Pts',(151.069477530402,-3.36816630900461,331.413434878276));
#51148=CARTESIAN_POINT('Ctrl Pts',(151.061716275476,-3.46682830695273,331.508721439558));
#51149=CARTESIAN_POINT('Ctrl Pts',(151.05395502055,-3.56124874754242,331.607848703164));
#51150=CARTESIAN_POINT('Ctrl Pts',(151.046181350145,-3.65582023006556,331.707134538086));
#51151=CARTESIAN_POINT('Ctrl Pts',(151.038407679741,-3.74613633893139,331.810273058389));
#51152=CARTESIAN_POINT('Ctrl Pts',(151.030634009336,-3.83188914194493,331.9168508524));
#51153=CARTESIAN_POINT('Ctrl Pts',(151.023222205159,-3.91365013134875,332.018467424461));
#51154=CARTESIAN_POINT('Ctrl Pts',(151.015810400982,-3.99126292648982,332.123210048434));
#51155=CARTESIAN_POINT('Ctrl Pts',(151.008398596804,-4.06449862595056,332.230697925082));
#51156=CARTESIAN_POINT('Ctrl Pts',(151.00050640211,-4.14248104222782,332.345152547666));
#51157=CARTESIAN_POINT('Ctrl Pts',(150.992614207416,-4.2157420164164,332.463074658565));
#51158=CARTESIAN_POINT('Ctrl Pts',(150.984722012722,-4.28396339709006,332.584044562726));
#51159=CARTESIAN_POINT('Ctrl Pts',(150.976840276783,-4.35209437062295,332.704854157274));
#51160=CARTESIAN_POINT('Ctrl Pts',(150.968958540845,-4.41519886088457,332.82870318226));
#51161=CARTESIAN_POINT('Ctrl Pts',(150.961076804906,-4.47300097256328,332.955141725706));
#51162=CARTESIAN_POINT('Ctrl Pts',(150.953203992128,-4.5307376446544,333.081437124103));
#51163=CARTESIAN_POINT('Ctrl Pts',(150.945331179351,-4.58318373356687,333.210315865706));
#51164=CARTESIAN_POINT('Ctrl Pts',(150.937458366573,-4.63010851960001,333.341302270084));
#51165=CARTESIAN_POINT('Ctrl Pts',(150.929488284068,-4.6776130680765,333.473907030225));
#51166=CARTESIAN_POINT('Ctrl Pts',(150.921518201563,-4.71945875524838,333.608671554959));
#51167=CARTESIAN_POINT('Ctrl Pts',(150.913548119057,-4.75545540311106,333.745078898288));
#51168=CARTESIAN_POINT('Ctrl Pts',(150.905689535788,-4.7909484678868,333.879577940842));
#51169=CARTESIAN_POINT('Ctrl Pts',(150.897830952519,-4.82075498173637,334.015673759918));
#51170=CARTESIAN_POINT('Ctrl Pts',(150.88997236925,-4.84474209496655,334.152853557076));
#51171=CARTESIAN_POINT('Ctrl Pts',(150.881946537126,-4.8692397095272,334.292952858064));
#51172=CARTESIAN_POINT('Ctrl Pts',(150.873920705003,-4.88766729808636,334.434182418524));
#51173=CARTESIAN_POINT('Ctrl Pts',(150.865894872879,-4.8999380593034,334.575983399511));
#51174=CARTESIAN_POINT('Ctrl Pts',(150.857869040755,-4.91220882052043,334.717784380498));
#51175=CARTESIAN_POINT('Ctrl Pts',(150.849843208632,-4.91832270088092,334.860156367047));
#51176=CARTESIAN_POINT('Ctrl Pts',(150.841817376508,-4.91824934725933,335.002533906699));
#51177=CARTESIAN_POINT('',(149.091817376546,-4.91824904199947,335.003069751012));
#51178=CARTESIAN_POINT('Ctrl Pts',(150.841817376458,-4.91824934725888,335.002533907583));
#51179=CARTESIAN_POINT('Ctrl Pts',(150.833275004512,-4.91817127259594,335.154074817202));
#51180=CARTESIAN_POINT('Ctrl Pts',(150.824732632566,-4.911085205369,335.305373671443));
#51181=CARTESIAN_POINT('Ctrl Pts',(150.81619026062,-4.89708260457338,335.455812490488));
#51182=CARTESIAN_POINT('Ctrl Pts',(150.807602559515,-4.88300570051299,335.60704959662));
#51183=CARTESIAN_POINT('Ctrl Pts',(150.799014858409,-4.86193875138165,335.757417279804));
#51184=CARTESIAN_POINT('Ctrl Pts',(150.790427157303,-4.83402492592403,335.906303524237));
#51185=CARTESIAN_POINT('Ctrl Pts',(150.781816020346,-4.80603492358686,336.055596079497));
#51186=CARTESIAN_POINT('Ctrl Pts',(150.773204883389,-4.77116074209068,336.20339887848));
#51187=CARTESIAN_POINT('Ctrl Pts',(150.764593746432,-4.72959553291164,336.349114212201));
#51188=CARTESIAN_POINT('Ctrl Pts',(150.755951736087,-4.68788130057508,336.49535197705));
#51189=CARTESIAN_POINT('Ctrl Pts',(150.747309725742,-4.63942809708577,336.63948706579));
#51190=CARTESIAN_POINT('Ctrl Pts',(150.738667715397,-4.58447845653032,336.780938051733));
#51191=CARTESIAN_POINT('Ctrl Pts',(150.735831997775,-4.56644773707678,336.827352605462));
#51192=CARTESIAN_POINT('Ctrl Pts',(150.732996280153,-4.54771791320033,336.873478355996));
#51193=CARTESIAN_POINT('Ctrl Pts',(150.730160562531,-4.52829862265166,336.919295351579));
#51194=CARTESIAN_POINT('Ctrl Pts',(150.722385483752,-4.47505407084348,337.044918138305));
#51195=CARTESIAN_POINT('Ctrl Pts',(150.714610404974,-4.41649393344499,337.168522111345));
#51196=CARTESIAN_POINT('Ctrl Pts',(150.706835326195,-4.35279236519956,337.289624791961));
#51197=CARTESIAN_POINT('Ctrl Pts',(150.699069815146,-4.28916918578925,337.410578448018));
#51198=CARTESIAN_POINT('Ctrl Pts',(150.691304304097,-4.22041734439196,337.529036593359));
#51199=CARTESIAN_POINT('Ctrl Pts',(150.683538793048,-4.14675933748497,337.64453588735));
#51200=CARTESIAN_POINT('Ctrl Pts',(150.675780981526,-4.07317436270628,337.759920663454));
#51201=CARTESIAN_POINT('Ctrl Pts',(150.668023170004,-3.9946931118216,337.872352099019));
#51202=CARTESIAN_POINT('Ctrl Pts',(150.660265358481,-3.9115841789396,337.981390996426));
#51203=CARTESIAN_POINT('Ctrl Pts',(150.652513384958,-3.82853778816521,338.090347838605));
#51204=CARTESIAN_POINT('Ctrl Pts',(150.644761411435,-3.74087088308443,338.195916914615));
#51205=CARTESIAN_POINT('Ctrl Pts',(150.637009437912,-3.64889538647973,338.29768790534));
#51206=CARTESIAN_POINT('Ctrl Pts',(150.629260747355,-3.55695884155242,338.399415795991));
#51207=CARTESIAN_POINT('Ctrl Pts',(150.621512056797,-3.46071759581903,338.497348511143));
#51208=CARTESIAN_POINT('Ctrl Pts',(150.61376336624,-3.36052373623727,338.591108920749));
#51209=CARTESIAN_POINT('Ctrl Pts',(150.606016287862,-3.26035072282476,338.684849822719));
#51210=CARTESIAN_POINT('Ctrl Pts',(150.598269209484,-3.15622701654611,338.774419878914));
#51211=CARTESIAN_POINT('Ctrl Pts',(150.590522131106,-3.04854114736669,338.859479231103));
#51212=CARTESIAN_POINT('Ctrl Pts',(150.5827749878,-2.94085437567601,338.944539296171));
#51213=CARTESIAN_POINT('Ctrl Pts',(150.575027844494,-2.82960568826708,339.025088339549));
#51214=CARTESIAN_POINT('Ctrl Pts',(150.567280701189,-2.71521591517816,339.100827428271));
#51215=CARTESIAN_POINT('Ctrl Pts',(150.559531816161,-2.60080042483987,339.176583544749));
#51216=CARTESIAN_POINT('Ctrl Pts',(150.551782931133,-2.48324276944337,339.247527338997));
#51217=CARTESIAN_POINT('Ctrl Pts',(150.544034046104,-2.36299156328245,339.313403984599));
#51218=CARTESIAN_POINT('Ctrl Pts',(150.53627693633,-2.24261272124873,339.379350552354));
#51219=CARTESIAN_POINT('Ctrl Pts',(150.528519826555,-2.1195349607506,339.440219039662));
#51220=CARTESIAN_POINT('Ctrl Pts',(150.52076271678,-1.99423072945102,339.495801025425));
#51221=CARTESIAN_POINT('Ctrl Pts',(150.513001461854,-1.8688595395767,339.551412712424));
#51222=CARTESIAN_POINT('Ctrl Pts',(150.505240206928,-1.74125987164417,339.601732125612));
#51223=CARTESIAN_POINT('Ctrl Pts',(150.497478952002,-1.61192188696308,339.646599928209));
#51224=CARTESIAN_POINT('Ctrl Pts',(150.489705281597,-1.48237700365775,339.691539504667));
#51225=CARTESIAN_POINT('Ctrl Pts',(150.481931611192,-1.35108862138193,339.731009931196));
#51226=CARTESIAN_POINT('Ctrl Pts',(150.474157940788,-1.21856057878688,339.764902221277));
#51227=CARTESIAN_POINT('Ctrl Pts',(150.466746136611,-1.09220174846003,339.7972168171));
#51228=CARTESIAN_POINT('Ctrl Pts',(150.459334332434,-0.964716354347555,
339.824460853759));
#51229=CARTESIAN_POINT('Ctrl Pts',(150.451922528257,-0.836545810924017,
339.846583762685));
#51230=CARTESIAN_POINT('Ctrl Pts',(150.444147449478,-0.70209324736589,339.869790981279));
#51231=CARTESIAN_POINT('Ctrl Pts',(150.4363723707,-0.566461778935172,339.887435714621));
#51232=CARTESIAN_POINT('Ctrl Pts',(150.428597291922,-0.43015137742047,339.899403316222));
#51233=CARTESIAN_POINT('Ctrl Pts',(150.420831780873,-0.294008714532869,
339.911356190926));
#51234=CARTESIAN_POINT('Ctrl Pts',(150.413066269824,-0.15718916656197,339.91764580031));
#51235=CARTESIAN_POINT('Ctrl Pts',(150.405300758775,-0.0202027721430652,
339.918208506204));
#51236=CARTESIAN_POINT('Ctrl Pts',(150.397542947252,0.116647799867042,339.918770654173));
#51237=CARTESIAN_POINT('Ctrl Pts',(150.38978513573,0.253664500759507,339.913617197079));
#51238=CARTESIAN_POINT('Ctrl Pts',(150.382027324208,0.390332648203933,339.902736326404));
#51239=CARTESIAN_POINT('Ctrl Pts',(150.374275350685,0.526897948533226,339.891863643931));
#51240=CARTESIAN_POINT('Ctrl Pts',(150.366523377162,0.663114829432412,339.875272157738));
#51241=CARTESIAN_POINT('Ctrl Pts',(150.358771403639,0.798469445487928,339.853002123132));
#51242=CARTESIAN_POINT('Ctrl Pts',(150.351022713081,0.933766738783276,339.830741519898));
#51243=CARTESIAN_POINT('Ctrl Pts',(150.343274022524,1.06820210864563,339.802807214691));
#51244=CARTESIAN_POINT('Ctrl Pts',(150.335525331966,1.20126788391611,339.769291198236));
#51245=CARTESIAN_POINT('Ctrl Pts',(150.327778253588,1.33430597374067,339.735782155068));
#51246=CARTESIAN_POINT('Ctrl Pts',(150.32003117521,1.46597465697226,339.696693806012));
#51247=CARTESIAN_POINT('Ctrl Pts',(150.312284096833,1.59577788371615,339.652168957416));
#51248=CARTESIAN_POINT('Ctrl Pts',(150.304536953527,1.72558219833606,339.607643735658));
#51249=CARTESIAN_POINT('Ctrl Pts',(150.296789810221,1.85352065555674,339.557682050305));
#51250=CARTESIAN_POINT('Ctrl Pts',(150.289042666915,1.97911414098799,339.502476016531));
#51251=CARTESIAN_POINT('Ctrl Pts',(150.281293781887,2.10473586250115,339.44725757127));
#51252=CARTESIAN_POINT('Ctrl Pts',(150.273544896859,2.22801120539586,339.386792588686));
#51253=CARTESIAN_POINT('Ctrl Pts',(150.265796011831,2.34848310976586,339.321320416915));
#51254=CARTESIAN_POINT('Ctrl Pts',(150.258038902056,2.46908288425991,339.255778752304));
#51255=CARTESIAN_POINT('Ctrl Pts',(150.250281792282,2.58687293221568,339.185219468868));
#51256=CARTESIAN_POINT('Ctrl Pts',(150.242524682507,2.70142231934475,339.10992706931));
#51257=CARTESIAN_POINT('Ctrl Pts',(150.234763427581,2.81603291800372,339.034594435901));
#51258=CARTESIAN_POINT('Ctrl Pts',(150.227002172654,2.92739908805709,338.95452387472));
#51259=CARTESIAN_POINT('Ctrl Pts',(150.219240917728,3.03512158539585,338.870041346596));
#51260=CARTESIAN_POINT('Ctrl Pts',(150.211467247324,3.14301640362368,338.78542367396));
#51261=CARTESIAN_POINT('Ctrl Pts',(150.203693576919,3.24725560433177,338.696380184997));
#51262=CARTESIAN_POINT('Ctrl Pts',(150.195919906514,3.34747488242671,338.603275589519));
#51263=CARTESIAN_POINT('Ctrl Pts',(150.188508102337,3.44302892901514,338.51450503536));
#51264=CARTESIAN_POINT('Ctrl Pts',(150.18109629816,3.53492868253356,338.422043159167));
#51265=CARTESIAN_POINT('Ctrl Pts',(150.173684493983,3.62289274409264,338.326233790235));
#51266=CARTESIAN_POINT('Ctrl Pts',(150.165909415205,3.71516818633996,338.22572851873));
#51267=CARTESIAN_POINT('Ctrl Pts',(150.158134336426,3.80340398914119,338.121221701023));
#51268=CARTESIAN_POINT('Ctrl Pts',(150.150359257648,3.88723318039331,338.013071732261));
#51269=CARTESIAN_POINT('Ctrl Pts',(150.142593746599,3.97095921448882,337.905054848921));
#51270=CARTESIAN_POINT('Ctrl Pts',(150.13482823555,4.05028918931382,337.79340404065));
#51271=CARTESIAN_POINT('Ctrl Pts',(150.127062724501,4.12489357900246,337.678513771554));
#51272=CARTESIAN_POINT('Ctrl Pts',(150.119304912978,4.19942399822149,337.563737416494));
#51273=CARTESIAN_POINT('Ctrl Pts',(150.111547101456,4.26923794507597,337.445728318251));
#51274=CARTESIAN_POINT('Ctrl Pts',(150.103789289934,4.33404696539169,337.324912893912));
#51275=CARTESIAN_POINT('Ctrl Pts',(150.096037316411,4.39880721486438,337.204188387011));
#51276=CARTESIAN_POINT('Ctrl Pts',(150.088285342888,4.45856985053881,337.080662100605));
#51277=CARTESIAN_POINT('Ctrl Pts',(150.080533369365,4.51309065272202,336.95478792272));
#51278=CARTESIAN_POINT('Ctrl Pts',(150.072784678807,4.56758836531311,336.828967052624));
#51279=CARTESIAN_POINT('Ctrl Pts',(150.06503598825,4.61684850464463,336.700800626637));
#51280=CARTESIAN_POINT('Ctrl Pts',(150.057287297692,4.66067369768583,336.570765337725));
#51281=CARTESIAN_POINT('Ctrl Pts',(150.049540219314,4.70448977252959,336.440757103742));
#51282=CARTESIAN_POINT('Ctrl Pts',(150.041793140937,4.74287302553924,336.308881150421));
#51283=CARTESIAN_POINT('Ctrl Pts',(150.034046062559,4.77567510455741,336.175631897411));
#51284=CARTESIAN_POINT('Ctrl Pts',(150.026298919253,4.80847745848857,336.042381527644));
#51285=CARTESIAN_POINT('Ctrl Pts',(150.018551775947,4.83569845169829,335.907758214774));
#51286=CARTESIAN_POINT('Ctrl Pts',(150.010804632641,4.85724036164861,335.772268820859));
#51287=CARTESIAN_POINT('Ctrl Pts',(150.003055747613,4.87878711467762,335.636748966052));
#51288=CARTESIAN_POINT('Ctrl Pts',(149.995306862585,4.89465218243718,335.500363028692));
#51289=CARTESIAN_POINT('Ctrl Pts',(149.987557977557,4.90478949653835,335.363624885214));
#51290=CARTESIAN_POINT('Ctrl Pts',(149.979800867782,4.91493757048945,335.226741606458));
#51291=CARTESIAN_POINT('Ctrl Pts',(149.972043758008,4.91934571747228,335.089505765234));
#51292=CARTESIAN_POINT('Ctrl Pts',(149.964286648233,4.91801997860885,334.952433704115));
#51293=CARTESIAN_POINT('Ctrl Pts',(149.956525393307,4.91669353131296,334.815288396069));
#51294=CARTESIAN_POINT('Ctrl Pts',(149.948764138381,4.90962711299133,334.678307432676));
#51295=CARTESIAN_POINT('Ctrl Pts',(149.941002883454,4.89687877716162,334.542002942931));
#51296=CARTESIAN_POINT('Ctrl Pts',(149.93322921305,4.88411004814925,334.405480410423));
#51297=CARTESIAN_POINT('Ctrl Pts',(149.925455542645,4.86564129136798,334.26963690151));
#51298=CARTESIAN_POINT('Ctrl Pts',(149.91768187224,4.8415820526893,334.134976133522));
#51299=CARTESIAN_POINT('Ctrl Pts',(149.910270068063,4.81864277735936,334.006583856681));
#51300=CARTESIAN_POINT('Ctrl Pts',(149.902858263886,4.79062184291682,333.879266966682));
#51301=CARTESIAN_POINT('Ctrl Pts',(149.895446459709,4.75765610166489,333.753448163617));
#51302=CARTESIAN_POINT('Ctrl Pts',(149.887671380931,4.72307461123441,333.621462606218));
#51303=CARTESIAN_POINT('Ctrl Pts',(149.879896302152,4.68294205453384,333.490708601553));
#51304=CARTESIAN_POINT('Ctrl Pts',(149.872121223374,4.6373612240282,333.36168869247));
#51305=CARTESIAN_POINT('Ctrl Pts',(149.864355712325,4.59183648363631,333.2328275506));
#51306=CARTESIAN_POINT('Ctrl Pts',(149.856590201276,4.54087693832692,333.105696623462));
#51307=CARTESIAN_POINT('Ctrl Pts',(149.848824690227,4.48463597602692,332.980786483547));
#51308=CARTESIAN_POINT('Ctrl Pts',(149.841066878704,4.42845077680477,332.8560001924));
#51309=CARTESIAN_POINT('Ctrl Pts',(149.833309067182,4.3669947410451,332.733430660655));
#51310=CARTESIAN_POINT('Ctrl Pts',(149.82555125566,4.30047035286795,332.613551214335));
#51311=CARTESIAN_POINT('Ctrl Pts',(149.817799282137,4.23399602640254,332.493761981099));
#51312=CARTESIAN_POINT('Ctrl Pts',(149.810047308614,4.16246112818873,332.376659144269));
#51313=CARTESIAN_POINT('Ctrl Pts',(149.802295335091,4.08611518106168,332.262693698251));
#51314=CARTESIAN_POINT('Ctrl Pts',(149.794546644533,4.00980156648857,332.148776516666));
#51315=CARTESIAN_POINT('Ctrl Pts',(149.786797953976,3.92868117250317,332.037994407293));
#51316=CARTESIAN_POINT('Ctrl Pts',(149.779049263418,3.84304805051992,331.930771311242));
#51317=CARTESIAN_POINT('Ctrl Pts',(149.77130218504,3.75743274522292,331.823570523852));
#51318=CARTESIAN_POINT('Ctrl Pts',(149.763555106662,3.66730682325951,331.719927582142));
#51319=CARTESIAN_POINT('Ctrl Pts',(149.755808028285,3.57300577079482,331.62023479745));
#51320=CARTESIAN_POINT('Ctrl Pts',(149.748060884979,3.47870392799654,331.520541177236));
#51321=CARTESIAN_POINT('Ctrl Pts',(149.740313741673,3.38022715350794,331.424798064034));
#51322=CARTESIAN_POINT('Ctrl Pts',(149.732566598367,3.27794879517396,331.333361926953));
#51323=CARTESIAN_POINT('Ctrl Pts',(149.724817713339,3.1756474424936,331.241905233087));
#51324=CARTESIAN_POINT('Ctrl Pts',(149.717068828311,3.06954309660301,331.154757702613));
#51325=CARTESIAN_POINT('Ctrl Pts',(149.709319943283,2.96004295691114,331.072236163446));
#51326=CARTESIAN_POINT('Ctrl Pts',(149.701562833508,2.85042659263962,330.989627035065));
#51327=CARTESIAN_POINT('Ctrl Pts',(149.693805723733,2.73740754722742,330.911653941946));
#51328=CARTESIAN_POINT('Ctrl Pts',(149.686048613959,2.6214232933585,330.838591226575));
#51329=CARTESIAN_POINT('Ctrl Pts',(149.678287359033,2.50537706121282,330.765489468825));
#51330=CARTESIAN_POINT('Ctrl Pts',(149.670526104106,2.38636280230974,330.697303511489));
#51331=CARTESIAN_POINT('Ctrl Pts',(149.66276484918,2.2648425929373,330.634261678511));
#51332=CARTESIAN_POINT('Ctrl Pts',(149.654991178776,2.14312799083321,330.571118999145));
#51333=CARTESIAN_POINT('Ctrl Pts',(149.647217508371,2.01889978206228,330.513137053365));
#51334=CARTESIAN_POINT('Ctrl Pts',(149.639443837966,1.89264083483156,330.460496312059));
#51335=CARTESIAN_POINT('Ctrl Pts',(149.632032033789,1.77225927197126,330.410306009927));
#51336=CARTESIAN_POINT('Ctrl Pts',(149.624620229612,1.65003204751828,330.36497093688));
#51337=CARTESIAN_POINT('Ctrl Pts',(149.617208425435,1.52638867762962,330.324604758172));
#51338=CARTESIAN_POINT('Ctrl Pts',(149.609433346657,1.3966851778673,330.282260112801));
#51339=CARTESIAN_POINT('Ctrl Pts',(149.601658267878,1.26501331659337,330.245249941333));
#51340=CARTESIAN_POINT('Ctrl Pts',(149.5938831891,1.13185131971292,330.213759758165));
#51341=CARTESIAN_POINT('Ctrl Pts',(149.586117678051,0.998853187147241,330.182308325671));
#51342=CARTESIAN_POINT('Ctrl Pts',(149.578352167002,0.86436894427227,330.15636345505));
#51343=CARTESIAN_POINT('Ctrl Pts',(149.570586655953,0.728894130971136,330.136061636047));
#51344=CARTESIAN_POINT('Ctrl Pts',(149.56282884443,0.593553641341721,330.115779946356));
#51345=CARTESIAN_POINT('Ctrl Pts',(149.555071032908,0.457224919894869,330.101130231268));
#51346=CARTESIAN_POINT('Ctrl Pts',(149.547313221386,0.320415572356604,330.092198361436));
#51347=CARTESIAN_POINT('Ctrl Pts',(149.539561247863,0.183709178190882,330.08327321312));
#51348=CARTESIAN_POINT('Ctrl Pts',(149.53180927434,0.0465232663262014,330.08005737079));
#51349=CARTESIAN_POINT('Ctrl Pts',(149.524057300817,-0.090627881296994,
330.082585064322));
#51350=CARTESIAN_POINT('Ctrl Pts',(149.516308610259,-0.227720945327791,
330.085111687374));
#51351=CARTESIAN_POINT('Ctrl Pts',(149.508559919702,-0.364778884404885,
330.093377001246));
#51352=CARTESIAN_POINT('Ctrl Pts',(149.500811229144,-0.501286069311462,
330.107363150691));
#51353=CARTESIAN_POINT('Ctrl Pts',(149.493064150766,-0.637764852758043,
330.121346390201));
#51354=CARTESIAN_POINT('Ctrl Pts',(149.485317072388,-0.773692721365163,
330.141048057943));
#51355=CARTESIAN_POINT('Ctrl Pts',(149.477569994011,-0.908558221347149,
330.166398338617));
#51356=CARTESIAN_POINT('Ctrl Pts',(149.469822850705,-1.04342485163183,330.191748831751));
#51357=CARTESIAN_POINT('Ctrl Pts',(149.462075707399,-1.17722871138541,330.222747960036));
#51358=CARTESIAN_POINT('Ctrl Pts',(149.454328564093,-1.30946799818671,330.259274673193));
#51359=CARTESIAN_POINT('Ctrl Pts',(149.446579679065,-1.44173701518701,330.295809598331));
#51360=CARTESIAN_POINT('Ctrl Pts',(149.438830794037,-1.57244038260137,330.337874477164));
#51361=CARTESIAN_POINT('Ctrl Pts',(149.431081909009,-1.70109131411029,330.385298340785));
#51362=CARTESIAN_POINT('Ctrl Pts',(149.423324799234,-1.82987879704736,330.432772540586));
#51363=CARTESIAN_POINT('Ctrl Pts',(149.415567689459,-1.95660912503818,330.485616952247));
#51364=CARTESIAN_POINT('Ctrl Pts',(149.407810579685,-2.08081485606185,330.543612158116));
#51365=CARTESIAN_POINT('Ctrl Pts',(149.400049324759,-2.20508695865685,330.601638354769));
#51366=CARTESIAN_POINT('Ctrl Pts',(149.392288069832,-2.32683142939363,330.664820650114));
#51367=CARTESIAN_POINT('Ctrl Pts',(149.384526814906,-2.44560620980308,330.732894033531));
#51368=CARTESIAN_POINT('Ctrl Pts',(149.376753144502,-2.56457099115257,330.801076312177));
#51369=CARTESIAN_POINT('Ctrl Pts',(149.368979474097,-2.68055625832943,330.87416510536));
#51370=CARTESIAN_POINT('Ctrl Pts',(149.361205803692,-2.79314894181757,330.951852022057));
#51371=CARTESIAN_POINT('Ctrl Pts',(149.353793999515,-2.90050040880148,331.025922594092));
#51372=CARTESIAN_POINT('Ctrl Pts',(149.346382195338,-3.00476780345651,331.104172665388));
#51373=CARTESIAN_POINT('Ctrl Pts',(149.338970391161,-3.10562310640945,331.186302557434));
#51374=CARTESIAN_POINT('Ctrl Pts',(149.331298440607,-3.21001832231312,331.271315120594));
#51375=CARTESIAN_POINT('Ctrl Pts',(149.323626490054,-3.31110645320642,331.36076925575));
#51376=CARTESIAN_POINT('Ctrl Pts',(149.315954539501,-3.408478394479,331.454374794642));
#51377=CARTESIAN_POINT('Ctrl Pts',(149.308292078548,-3.50572989430311,331.54786455083));
#51378=CARTESIAN_POINT('Ctrl Pts',(149.300629617595,-3.59927405891711,331.645495223002));
#51379=CARTESIAN_POINT('Ctrl Pts',(149.292967156642,-3.68873314137439,331.746935156775));
#51380=CARTESIAN_POINT('Ctrl Pts',(149.285312223662,-3.77810433489762,331.848275431046));
#51381=CARTESIAN_POINT('Ctrl Pts',(149.277657290682,-3.86339816508794,331.953417223214));
#51382=CARTESIAN_POINT('Ctrl Pts',(149.270002357702,-3.94427257793943,332.061990998411));
#51383=CARTESIAN_POINT('Ctrl Pts',(149.262353071697,-4.02508733046593,332.170484679714));
#51384=CARTESIAN_POINT('Ctrl Pts',(149.254703785692,-4.10148891324412,332.28240498521));
#51385=CARTESIAN_POINT('Ctrl Pts',(149.247054499687,-4.17317488513449,332.397348574899));
#51386=CARTESIAN_POINT('Ctrl Pts',(149.239408214288,-4.24483273657044,332.512247075347));
#51387=CARTESIAN_POINT('Ctrl Pts',(149.231761928889,-4.31177844248423,332.630166161405));
#51388=CARTESIAN_POINT('Ctrl Pts',(149.224115643491,-4.37375254171764,332.750673041481));
#51389=CARTESIAN_POINT('Ctrl Pts',(149.216470598857,-4.43571658439673,332.871160366873));
#51390=CARTESIAN_POINT('Ctrl Pts',(149.208825554224,-4.49271044121826,332.994234293507));
#51391=CARTESIAN_POINT('Ctrl Pts',(149.20118050959,-4.54452059642395,333.119437421627));
#51392=CARTESIAN_POINT('Ctrl Pts',(149.193534947129,-4.59633426092566,333.244649030223));
#51393=CARTESIAN_POINT('Ctrl Pts',(149.185889384667,-4.64296337287306,333.371989755078));
#51394=CARTESIAN_POINT('Ctrl Pts',(149.178243822206,-4.68424276676859,333.500982733763));
#51395=CARTESIAN_POINT('Ctrl Pts',(149.170592019132,-4.7255558545542,333.630081001669));
#51396=CARTESIAN_POINT('Ctrl Pts',(149.162940216057,-4.76151038023566,333.760833833398));
#51397=CARTESIAN_POINT('Ctrl Pts',(149.155288412982,-4.79199117641293,333.892749518997));
#51398=CARTESIAN_POINT('Ctrl Pts',(149.147633370225,-4.82248487779625,334.024721056127));
#51399=CARTESIAN_POINT('Ctrl Pts',(149.139978327468,-4.84750015936146,334.157856032681));
#51400=CARTESIAN_POINT('Ctrl Pts',(149.132323284711,-4.86697334089238,334.291654348822));
#51401=CARTESIAN_POINT('Ctrl Pts',(149.124657930291,-4.88647275361318,334.42563289689));
#51402=CARTESIAN_POINT('Ctrl Pts',(149.116992575872,-4.90041511348892,334.560276169459));
#51403=CARTESIAN_POINT('Ctrl Pts',(149.109327221452,-4.90878875424659,334.695080291417));
#51404=CARTESIAN_POINT('Ctrl Pts',(149.103490606483,-4.91516467821747,334.797723915313));
#51405=CARTESIAN_POINT('Ctrl Pts',(149.097653991514,-4.91831308596907,334.900460715021));
#51406=CARTESIAN_POINT('Ctrl Pts',(149.091817376545,-4.91824904199947,335.003069751012));
#51407=CARTESIAN_POINT('',(147.341817376463,-4.91824822950257,334.995826812387));
#51408=CARTESIAN_POINT('Ctrl Pts',(149.091817376508,-4.91824904199906,335.003069751671));
#51409=CARTESIAN_POINT('Ctrl Pts',(149.081455703301,-4.91813534547636,335.185230354129));
#51410=CARTESIAN_POINT('Ctrl Pts',(149.071094030094,-4.90790203713303,335.367074026762));
#51411=CARTESIAN_POINT('Ctrl Pts',(149.060732356887,-4.88765040461514,335.547774209657));
#51412=CARTESIAN_POINT('Ctrl Pts',(149.052957278108,-4.87245420656191,335.683366032445));
#51413=CARTESIAN_POINT('Ctrl Pts',(149.04518219933,-4.85158739502761,335.81853928431));
#51414=CARTESIAN_POINT('Ctrl Pts',(149.037407120552,-4.82507925338847,335.952781853847));
#51415=CARTESIAN_POINT('Ctrl Pts',(149.029641609503,-4.79860373170523,336.086859229356));
#51416=CARTESIAN_POINT('Ctrl Pts',(149.021876098454,-4.76650076753593,336.22000782148));
#51417=CARTESIAN_POINT('Ctrl Pts',(149.014110587405,-4.72885143676541,336.351720071428));
#51418=CARTESIAN_POINT('Ctrl Pts',(149.006352775883,-4.69123943541598,336.483301728297));
#51419=CARTESIAN_POINT('Ctrl Pts',(148.998594964361,-4.64809211799609,336.613449503702));
#51420=CARTESIAN_POINT('Ctrl Pts',(148.990837152838,-4.59954162977641,336.741665828583));
#51421=CARTESIAN_POINT('Ctrl Pts',(148.983085179315,-4.55102767733875,336.869785666614));
#51422=CARTESIAN_POINT('Ctrl Pts',(148.975333205792,-4.49711878525,336.995976583124));
#51423=CARTESIAN_POINT('Ctrl Pts',(148.967581232269,-4.43799686513836,337.119756327393));
#51424=CARTESIAN_POINT('Ctrl Pts',(148.959832541712,-4.37889998319499,337.243483650866));
#51425=CARTESIAN_POINT('Ctrl Pts',(148.952083851154,-4.31459463234466,337.364801481087));
#51426=CARTESIAN_POINT('Ctrl Pts',(148.944335160597,-4.24531068722392,337.483247919851));
#51427=CARTESIAN_POINT('Ctrl Pts',(148.936588082219,-4.17604115720661,337.601669714844));
#51428=CARTESIAN_POINT('Ctrl Pts',(148.928841003841,-4.10179529050457,337.717220969504));
#51429=CARTESIAN_POINT('Ctrl Pts',(148.921093925463,-4.02284852288737,337.829465112774));
#51430=CARTESIAN_POINT('Ctrl Pts',(148.913346782157,-3.9439010936203,337.941710196758));
#51431=CARTESIAN_POINT('Ctrl Pts',(148.905599638851,-3.86025290972531,338.050647794355));
#51432=CARTESIAN_POINT('Ctrl Pts',(148.897852495546,-3.77222203952135,338.155871345136));
#51433=CARTESIAN_POINT('Ctrl Pts',(148.890103610518,-3.68417137810882,338.261118552405));
#51434=CARTESIAN_POINT('Ctrl Pts',(148.882354725489,-3.59173632047028,338.36264975157));
#51435=CARTESIAN_POINT('Ctrl Pts',(148.874605840461,-3.49527414681052,338.460092730136));
#51436=CARTESIAN_POINT('Ctrl Pts',(148.866848730687,-3.39870958720293,338.557639135686));
#51437=CARTESIAN_POINT('Ctrl Pts',(148.859091620912,-3.29810964843672,338.651088374295));
#51438=CARTESIAN_POINT('Ctrl Pts',(148.851334511137,-3.1938676916432,338.740105911706));
#51439=CARTESIAN_POINT('Ctrl Pts',(148.843573256211,-3.08957003128094,338.829171017243));
#51440=CARTESIAN_POINT('Ctrl Pts',(148.835812001285,-2.98162678240673,338.913799461767));
#51441=CARTESIAN_POINT('Ctrl Pts',(148.828050746359,-2.87046228586948,338.993698702694));
#51442=CARTESIAN_POINT('Ctrl Pts',(148.820277075954,-2.7591199623663,339.073725756368));
#51443=CARTESIAN_POINT('Ctrl Pts',(148.812503405549,-2.644546420926,339.149008274211));
#51444=CARTESIAN_POINT('Ctrl Pts',(148.804729735145,-2.52719347465679,339.219298070077));
#51445=CARTESIAN_POINT('Ctrl Pts',(148.797317930967,-2.41530333626886,339.286315859035));
#51446=CARTESIAN_POINT('Ctrl Pts',(148.78990612679,-2.30088698494053,339.348795149962));
#51447=CARTESIAN_POINT('Ctrl Pts',(148.782494322613,-2.1843530681089,339.406561554812));
#51448=CARTESIAN_POINT('Ctrl Pts',(148.774719243835,-2.06210747687777,339.46715926324));
#51449=CARTESIAN_POINT('Ctrl Pts',(148.766944165056,-1.93714517653106,339.52276191907));
#51450=CARTESIAN_POINT('Ctrl Pts',(148.759169086278,-1.80991265938974,339.573117014453));
#51451=CARTESIAN_POINT('Ctrl Pts',(148.751403575229,-1.68283670996075,339.623410144685));
#51452=CARTESIAN_POINT('Ctrl Pts',(148.74363806418,-1.55349646226297,339.668468420492));
#51453=CARTESIAN_POINT('Ctrl Pts',(148.735872553131,-1.42236260812602,339.708085351128));
#51454=CARTESIAN_POINT('Ctrl Pts',(148.728114741609,-1.29135877358727,339.747663001462));
#51455=CARTESIAN_POINT('Ctrl Pts',(148.720356930086,-1.15856524341956,339.781809930885));
#51456=CARTESIAN_POINT('Ctrl Pts',(148.712599118564,-1.02447194544925,339.810368000007));
#51457=CARTESIAN_POINT('Ctrl Pts',(148.704847145041,-0.890479556938012,
339.838904578275));
#51458=CARTESIAN_POINT('Ctrl Pts',(148.697095171518,-0.755189728278357,
339.861860586579));
#51459=CARTESIAN_POINT('Ctrl Pts',(148.689343197995,-0.619106437210259,
339.87912802475));
#51460=CARTESIAN_POINT('Ctrl Pts',(148.681594507437,-0.483080777496722,
339.896388150151));
#51461=CARTESIAN_POINT('Ctrl Pts',(148.67384581688,-0.34626271067641,339.907964447875));
#51462=CARTESIAN_POINT('Ctrl Pts',(148.666097126322,-0.20916505515901,339.913800264785));
#51463=CARTESIAN_POINT('Ctrl Pts',(148.658350047944,-0.0720959239539022,
339.919634867505));
#51464=CARTESIAN_POINT('Ctrl Pts',(148.650602969567,0.0652522899670618,
339.919731348455));
#51465=CARTESIAN_POINT('Ctrl Pts',(148.642855891189,0.202363410588895,339.914085073801));
#51466=CARTESIAN_POINT('Ctrl Pts',(148.635108747883,0.33947568033384,339.908438751826));
#51467=CARTESIAN_POINT('Ctrl Pts',(148.627361604577,0.476350462273005,339.897049594331));
#51468=CARTESIAN_POINT('Ctrl Pts',(148.619614461271,0.612473746048041,339.879965058574));
#51469=CARTESIAN_POINT('Ctrl Pts',(148.611865576243,0.74862763322711,339.86287668185));
#51470=CARTESIAN_POINT('Ctrl Pts',(148.604116691215,0.884029298289136,339.840090427594));
#51471=CARTESIAN_POINT('Ctrl Pts',(148.596367806187,1.01817239498544,339.811705314812));
#51472=CARTESIAN_POINT('Ctrl Pts',(148.588610696412,1.15245787255071,339.783290073778));
#51473=CARTESIAN_POINT('Ctrl Pts',(148.580853586638,1.28548173023891,339.749264184192));
#51474=CARTESIAN_POINT('Ctrl Pts',(148.573096476863,1.41674978077693,339.709777396138));
#51475=CARTESIAN_POINT('Ctrl Pts',(148.565335221937,1.54808797676402,339.670269507607));
#51476=CARTESIAN_POINT('Ctrl Pts',(148.557573967011,1.67766812698108,339.625295034071));
#51477=CARTESIAN_POINT('Ctrl Pts',(148.549812712084,1.80501459094619,339.575052501226));
#51478=CARTESIAN_POINT('Ctrl Pts',(148.54203904168,1.93256476775153,339.524729596702));
#51479=CARTESIAN_POINT('Ctrl Pts',(148.534265371275,2.05787376058951,339.4691219515));
#51480=CARTESIAN_POINT('Ctrl Pts',(148.52649170087,2.18048836243721,339.408475197137));
#51481=CARTESIAN_POINT('Ctrl Pts',(148.519079896693,2.2973952250702,339.350651563781));
#51482=CARTESIAN_POINT('Ctrl Pts',(148.511668092516,2.41185264666031,339.288247542365));
#51483=CARTESIAN_POINT('Ctrl Pts',(148.504256288339,2.52349283800256,339.221512401859));
#51484=CARTESIAN_POINT('Ctrl Pts',(148.496481209561,2.64060484768084,339.151506373324));
#51485=CARTESIAN_POINT('Ctrl Pts',(148.488706130782,2.75498657825241,339.076512696558));
#51486=CARTESIAN_POINT('Ctrl Pts',(148.480931052004,2.86618406786426,338.996770189994));
#51487=CARTESIAN_POINT('Ctrl Pts',(148.473165540955,2.97724472188597,338.91712581166));
#51488=CARTESIAN_POINT('Ctrl Pts',(148.465400029906,3.0851286168589,338.8327444565));
#51489=CARTESIAN_POINT('Ctrl Pts',(148.457634518857,3.18940739195331,338.743910195324));
#51490=CARTESIAN_POINT('Ctrl Pts',(148.449876707334,3.29358277433861,338.655164013577));
#51491=CARTESIAN_POINT('Ctrl Pts',(148.442118895812,3.39415985464853,338.561973963895));
#51492=CARTESIAN_POINT('Ctrl Pts',(148.43436108429,3.49074052203594,338.46466645874));
#51493=CARTESIAN_POINT('Ctrl Pts',(148.426609110767,3.58724850940835,338.367432180568));
#51494=CARTESIAN_POINT('Ctrl Pts',(148.418857137244,3.67976579575248,338.266086890675));
#51495=CARTESIAN_POINT('Ctrl Pts',(148.411105163721,3.76792883014986,338.160995949606));
#51496=CARTESIAN_POINT('Ctrl Pts',(148.403356473163,3.85605452744983,338.055949514613));
#51497=CARTESIAN_POINT('Ctrl Pts',(148.395607782606,3.9398293897504,337.947160882284));
#51498=CARTESIAN_POINT('Ctrl Pts',(148.387859092048,4.01892826075413,337.835030634299));
#51499=CARTESIAN_POINT('Ctrl Pts',(148.38011201367,4.09801067457713,337.722923715948));
#51500=CARTESIAN_POINT('Ctrl Pts',(148.372364935293,4.17241880705802,337.607476884044));
#51501=CARTESIAN_POINT('Ctrl Pts',(148.364617856915,4.2418694290466,337.489121694377));
#51502=CARTESIAN_POINT('Ctrl Pts',(148.356870713609,4.31132063309823,337.37076551278));
#51503=CARTESIAN_POINT('Ctrl Pts',(148.349123570303,4.37581404596444,337.249501261922));
#51504=CARTESIAN_POINT('Ctrl Pts',(148.341376426997,4.43511141496652,337.125786865924));
#51505=CARTESIAN_POINT('Ctrl Pts',(148.333627541969,4.49442211527608,337.002044656303));
#51506=CARTESIAN_POINT('Ctrl Pts',(148.325878656941,4.54853427825956,336.875851557831));
#51507=CARTESIAN_POINT('Ctrl Pts',(148.318129771913,4.59725715810314,336.747686952738));
#51508=CARTESIAN_POINT('Ctrl Pts',(148.310372662138,4.64603175291481,336.619386312408));
#51509=CARTESIAN_POINT('Ctrl Pts',(148.302615552364,4.68940549875342,336.489110351278));
#51510=CARTESIAN_POINT('Ctrl Pts',(148.294858442589,4.7272368905704,336.357355680332));
#51511=CARTESIAN_POINT('Ctrl Pts',(148.287097187663,4.76508849827353,336.225530603903));
#51512=CARTESIAN_POINT('Ctrl Pts',(148.279335932736,4.7973917585791,336.092225622849));
#51513=CARTESIAN_POINT('Ctrl Pts',(148.27157467781,4.82405621962199,335.957948147045));
#51514=CARTESIAN_POINT('Ctrl Pts',(148.263801007406,4.85076333511261,335.82345587104));
#51515=CARTESIAN_POINT('Ctrl Pts',(148.256027337001,4.87181356617842,335.687988378028));
#51516=CARTESIAN_POINT('Ctrl Pts',(148.248253666596,4.88716821327738,335.55205970477));
#51517=CARTESIAN_POINT('Ctrl Pts',(148.240841862419,4.90180809785978,335.422458543956));
#51518=CARTESIAN_POINT('Ctrl Pts',(148.233430058242,4.91127070330743,335.292438459569));
#51519=CARTESIAN_POINT('Ctrl Pts',(148.226018254065,4.91556661337236,335.162443627142));
#51520=CARTESIAN_POINT('Ctrl Pts',(148.218243175287,4.92007307878642,335.026077360743));
#51521=CARTESIAN_POINT('Ctrl Pts',(148.210468096508,4.91890781370885,334.889307941644));
#51522=CARTESIAN_POINT('Ctrl Pts',(148.20269301773,4.91202598084666,334.752646354409));
#51523=CARTESIAN_POINT('Ctrl Pts',(148.194927506681,4.90515261651792,334.616152937957));
#51524=CARTESIAN_POINT('Ctrl Pts',(148.187161995632,4.89257670071302,334.479767475994));
#51525=CARTESIAN_POINT('Ctrl Pts',(148.179396484583,4.87430530401293,334.344003913296));
#51526=CARTESIAN_POINT('Ctrl Pts',(148.17163867306,4.85605202345587,334.208374960565));
#51527=CARTESIAN_POINT('Ctrl Pts',(148.163880861538,4.83211455182281,334.073367064888));
#51528=CARTESIAN_POINT('Ctrl Pts',(148.156123050016,4.80255193569416,333.939491646681));
#51529=CARTESIAN_POINT('Ctrl Pts',(148.148371076493,4.77301156637163,333.805716973971));
#51530=CARTESIAN_POINT('Ctrl Pts',(148.14061910297,4.73785456227512,333.673073462562));
#51531=CARTESIAN_POINT('Ctrl Pts',(148.132867129447,4.69719142461954,333.542064547732));
#51532=CARTESIAN_POINT('Ctrl Pts',(148.125118438889,4.65654550782691,333.411111115255));
#51533=CARTESIAN_POINT('Ctrl Pts',(148.117369748332,4.61039821098941,333.281791275045));
#51534=CARTESIAN_POINT('Ctrl Pts',(148.109621057774,4.55891043105675,333.1545952357));
#51535=CARTESIAN_POINT('Ctrl Pts',(148.101873979396,4.50743336358673,333.027425660553));
#51536=CARTESIAN_POINT('Ctrl Pts',(148.094126901019,4.45061816971201,332.902379369441));
#51537=CARTESIAN_POINT('Ctrl Pts',(148.086379822641,4.38867448235786,332.779928075399));
#51538=CARTESIAN_POINT('Ctrl Pts',(148.078632679335,4.32673027585597,332.657475755097));
#51539=CARTESIAN_POINT('Ctrl Pts',(148.070885536029,4.25965766658299,332.537618824031));
#51540=CARTESIAN_POINT('Ctrl Pts',(148.063138392723,4.18771280050651,332.420805442978));
#51541=CARTESIAN_POINT('Ctrl Pts',(148.055389507695,4.11575175969674,332.303965799797));
#51542=CARTESIAN_POINT('Ctrl Pts',(148.047640622667,4.03891648732571,332.19017140097));
#51543=CARTESIAN_POINT('Ctrl Pts',(148.039891737639,3.95750688263241,332.079842069953));
#51544=CARTESIAN_POINT('Ctrl Pts',(148.032134627864,3.87601086894355,331.969395634244));
#51545=CARTESIAN_POINT('Ctrl Pts',(148.024377518089,3.78993105657182,331.862421928229));
#51546=CARTESIAN_POINT('Ctrl Pts',(148.016620408315,3.69960847978766,331.759308691223));
#51547=CARTESIAN_POINT('Ctrl Pts',(148.008859153389,3.60923763750641,331.656140353799));
#51548=CARTESIAN_POINT('Ctrl Pts',(148.001097898462,3.51461978271333,331.556836878762));
#51549=CARTESIAN_POINT('Ctrl Pts',(147.993336643536,3.41613265850166,331.461748917612));
#51550=CARTESIAN_POINT('Ctrl Pts',(147.985562973132,3.31748798698816,331.366508846713));
#51551=CARTESIAN_POINT('Ctrl Pts',(147.977789302727,3.21496196993356,331.275498024731));
#51552=CARTESIAN_POINT('Ctrl Pts',(147.970015632322,3.10896592927525,331.189027169723));
#51553=CARTESIAN_POINT('Ctrl Pts',(147.962603828145,3.00790402981133,331.106581553821));
#51554=CARTESIAN_POINT('Ctrl Pts',(147.955192023968,2.90368812576625,331.028262918812));
#51555=CARTESIAN_POINT('Ctrl Pts',(147.947780219791,2.79669746129601,330.954302733461));
#51556=CARTESIAN_POINT('Ctrl Pts',(147.940005141013,2.68446286565063,330.87671753911));
#51557=CARTESIAN_POINT('Ctrl Pts',(147.932230062234,2.56881995148624,330.803683654871));
#51558=CARTESIAN_POINT('Ctrl Pts',(147.924454983456,2.45017415259188,330.735515308449));
#51559=CARTESIAN_POINT('Ctrl Pts',(147.916689472407,2.33167435490649,330.667430847517));
#51560=CARTESIAN_POINT('Ctrl Pts',(147.908923961358,2.21017936063772,330.604200204149));
#51561=CARTESIAN_POINT('Ctrl Pts',(147.901158450309,2.08612518320945,330.54609555755));
#51562=CARTESIAN_POINT('Ctrl Pts',(147.893400638787,1.96219400585928,330.488048521877));
#51563=CARTESIAN_POINT('Ctrl Pts',(147.885642827264,1.8357090466844,330.435117533354));
#51564=CARTESIAN_POINT('Ctrl Pts',(147.877885015742,1.70713232351747,330.387529697385));
#51565=CARTESIAN_POINT('Ctrl Pts',(147.870133042219,1.57865235841213,330.339977672773));
#51566=CARTESIAN_POINT('Ctrl Pts',(147.862381068696,1.4480841276178,330.297760932452));
#51567=CARTESIAN_POINT('Ctrl Pts',(147.854629095173,1.31591077914885,330.261058991313));
#51568=CARTESIAN_POINT('Ctrl Pts',(147.846880404616,1.1837934061714,330.224372593466));
#51569=CARTESIAN_POINT('Ctrl Pts',(147.839131714058,1.05007264337058,330.193196453978));
#51570=CARTESIAN_POINT('Ctrl Pts',(147.8313830235,0.915247788187289,330.16766055117));
#51571=CARTESIAN_POINT('Ctrl Pts',(147.823635945122,0.780450984441242,330.14212996132));
#51572=CARTESIAN_POINT('Ctrl Pts',(147.815888866745,0.64455092903888,330.122237346673));
#51573=CARTESIAN_POINT('Ctrl Pts',(147.808141788367,0.508057739939603,330.10806169342));
#51574=CARTESIAN_POINT('Ctrl Pts',(147.800394645061,0.371563406896028,330.093885921361));
#51575=CARTESIAN_POINT('Ctrl Pts',(147.792647501755,0.234476319023631,330.08542724664));
#51576=CARTESIAN_POINT('Ctrl Pts',(147.784900358449,0.097311959562549,330.082712796162));
#51577=CARTESIAN_POINT('Ctrl Pts',(147.777151473421,-0.0398832373586683,
330.079997735418));
#51578=CARTESIAN_POINT('Ctrl Pts',(147.769402588393,-0.177155349716091,
330.083029476437));
#51579=CARTESIAN_POINT('Ctrl Pts',(147.761653703365,-0.313989046323042,
330.091783018112));
#51580=CARTESIAN_POINT('Ctrl Pts',(147.75389659359,-0.450967979629376,330.100545850887));
#51581=CARTESIAN_POINT('Ctrl Pts',(147.746139483816,-0.587507176933875,
330.115042591069));
#51582=CARTESIAN_POINT('Ctrl Pts',(147.738382374041,-0.723096026763421,
330.135196283653));
#51583=CARTESIAN_POINT('Ctrl Pts',(147.730621119115,-0.858757330939025,
330.155360745727));
#51584=CARTESIAN_POINT('Ctrl Pts',(147.722859864189,-0.993466892044418,
330.181188110031));
#51585=CARTESIAN_POINT('Ctrl Pts',(147.715098609262,-1.12672542128919,330.212550481987));
#51586=CARTESIAN_POINT('Ctrl Pts',(147.707324938858,-1.26019712075186,330.243963023517));
#51587=CARTESIAN_POINT('Ctrl Pts',(147.699551268453,-1.39221277335739,330.280928160581));
#51588=CARTESIAN_POINT('Ctrl Pts',(147.691777598048,-1.52228849975986,330.323268151155));
#51589=CARTESIAN_POINT('Ctrl Pts',(147.684365793871,-1.6463091698045,330.363637204982));
#51590=CARTESIAN_POINT('Ctrl Pts',(147.676953989694,-1.76856618642563,330.408891874718));
#51591=CARTESIAN_POINT('Ctrl Pts',(147.669542185517,-1.8886596718276,330.458838506889));
#51592=CARTESIAN_POINT('Ctrl Pts',(147.661767106739,-2.01463929668861,330.511233172287));
#51593=CARTESIAN_POINT('Ctrl Pts',(147.65399202796,-2.13863606449778,330.568956940496));
#51594=CARTESIAN_POINT('Ctrl Pts',(147.646216949182,-2.26016633098809,330.631838920236));
#51595=CARTESIAN_POINT('Ctrl Pts',(147.638451438133,-2.38154704674857,330.694643519696));
#51596=CARTESIAN_POINT('Ctrl Pts',(147.630685927084,-2.50046695650412,330.762593523059));
#51597=CARTESIAN_POINT('Ctrl Pts',(147.622920416035,-2.61646122707147,330.835469569119));
#51598=CARTESIAN_POINT('Ctrl Pts',(147.615162604513,-2.73234048898173,330.908273358368));
#51599=CARTESIAN_POINT('Ctrl Pts',(147.60740479299,-2.84529955557861,330.985993263907));
#51600=CARTESIAN_POINT('Ctrl Pts',(147.599646981468,-2.95489742472289,331.068363664851));
#51601=CARTESIAN_POINT('Ctrl Pts',(147.591895007945,-3.06441281799505,331.150672079455));
#51602=CARTESIAN_POINT('Ctrl Pts',(147.584143034422,-3.17057173727117,331.237623789698));
#51603=CARTESIAN_POINT('Ctrl Pts',(147.576391060899,-3.27296176553896,331.328909651913));
#51604=CARTESIAN_POINT('Ctrl Pts',(147.568642370342,-3.37530843156909,331.42015685451));
#51605=CARTESIAN_POINT('Ctrl Pts',(147.560893679784,-3.47388909002619,331.515734298793));
#51606=CARTESIAN_POINT('Ctrl Pts',(147.553144989226,-3.56832424087003,331.61529245362));
#51607=CARTESIAN_POINT('Ctrl Pts',(147.545397910849,-3.66273974369194,331.714829894542));
#51608=CARTESIAN_POINT('Ctrl Pts',(147.537650832471,-3.75301118566073,331.818346115207));
#51609=CARTESIAN_POINT('Ctrl Pts',(147.529903754093,-3.8387960915049,331.925454890501));
#51610=CARTESIAN_POINT('Ctrl Pts',(147.522156610787,-3.9245817163092,332.032564563469));
#51611=CARTESIAN_POINT('Ctrl Pts',(147.514409467481,-4.00588048564268,332.143266546036));
#51612=CARTESIAN_POINT('Ctrl Pts',(147.506662324176,-4.08239063035362,332.257142037272));
#51613=CARTESIAN_POINT('Ctrl Pts',(147.498913439147,-4.15891797616937,332.371043130135));
#51614=CARTESIAN_POINT('Ctrl Pts',(147.491164554119,-4.23065433713573,332.488118827016));
#51615=CARTESIAN_POINT('Ctrl Pts',(147.483415669091,-4.29734186194209,332.60792224539));
#51616=CARTESIAN_POINT('Ctrl Pts',(147.475658559317,-4.36410016957633,332.727852824351));
#51617=CARTESIAN_POINT('Ctrl Pts',(147.467901449542,-4.42579874576242,332.850516566235));
#51618=CARTESIAN_POINT('Ctrl Pts',(147.460144339767,-4.48222598243681,332.975442442194));
#51619=CARTESIAN_POINT('Ctrl Pts',(147.452383084841,-4.53868337202223,333.100435074547));
#51620=CARTESIAN_POINT('Ctrl Pts',(147.444621829915,-4.58986366352323,333.227691887182));
#51621=CARTESIAN_POINT('Ctrl Pts',(147.436860574989,-4.63560421240568,333.356723806408));
#51622=CARTESIAN_POINT('Ctrl Pts',(147.429086904584,-4.68141793125959,333.485962134653));
#51623=CARTESIAN_POINT('Ctrl Pts',(147.421313234179,-4.72177440356769,333.616980870084));
#51624=CARTESIAN_POINT('Ctrl Pts',(147.413539563775,-4.75656124150922,333.749276921828));
#51625=CARTESIAN_POINT('Ctrl Pts',(147.406127759598,-4.78972874377483,333.875414560533));
#51626=CARTESIAN_POINT('Ctrl Pts',(147.398715955421,-4.81783341332766,334.002712992552));
#51627=CARTESIAN_POINT('Ctrl Pts',(147.391304151244,-4.84082170068331,334.130731155112));
#51628=CARTESIAN_POINT('Ctrl Pts',(147.379424478014,-4.87766743154478,334.335919244597));
#51629=CARTESIAN_POINT('Ctrl Pts',(147.367544804784,-4.9014749885021,334.54351405225));
#51630=CARTESIAN_POINT('Ctrl Pts',(147.355665131553,-4.91200260903515,334.752182665393));
#51631=CARTESIAN_POINT('Ctrl Pts',(147.351049213205,-4.91609317919156,334.833262107687));
#51632=CARTESIAN_POINT('Ctrl Pts',(147.346433294857,-4.91817922566193,334.914503377089));
#51633=CARTESIAN_POINT('Ctrl Pts',(147.341817376508,-4.9182482295019,334.995826811598));
#51634=CARTESIAN_POINT('',(145.591817376546,-4.91824992125433,334.999119896715));
#51635=CARTESIAN_POINT('Ctrl Pts',(147.341817376463,-4.91824822950257,334.995826812387));
#51636=CARTESIAN_POINT('Ctrl Pts',(147.334169792718,-4.91836255399992,335.13056224939));
#51637=CARTESIAN_POINT('Ctrl Pts',(147.326522208973,-4.91293610271415,335.265491128996));
#51638=CARTESIAN_POINT('Ctrl Pts',(147.318874625228,-4.90194789167757,335.400112396431));
#51639=CARTESIAN_POINT('Ctrl Pts',(147.311234006876,-4.8909696886645,335.534611051295));
#51640=CARTESIAN_POINT('Ctrl Pts',(147.303593388523,-4.87443983411927,335.668802251474));
#51641=CARTESIAN_POINT('Ctrl Pts',(147.29595277017,-4.85238939625965,335.80218464805));
#51642=CARTESIAN_POINT('Ctrl Pts',(147.288316847756,-4.83035251064086,335.935485067552));
#51643=CARTESIAN_POINT('Ctrl Pts',(147.280680925341,-4.80280185530966,336.067977275241));
#51644=CARTESIAN_POINT('Ctrl Pts',(147.273045002927,-4.76982031462235,336.199165221609));
#51645=CARTESIAN_POINT('Ctrl Pts',(147.265411530115,-4.73684935440743,336.330311082906));
#51646=CARTESIAN_POINT('Ctrl Pts',(147.257778057303,-4.69845107032931,336.460153123703));
#51647=CARTESIAN_POINT('Ctrl Pts',(147.250144584491,-4.65475932115117,336.588206134183));
#51648=CARTESIAN_POINT('Ctrl Pts',(147.242511794147,-4.61107147821453,336.71624769614));
#51649=CARTESIAN_POINT('Ctrl Pts',(147.234879003802,-4.56209124152275,336.842500163918));
#51650=CARTESIAN_POINT('Ctrl Pts',(147.227246213458,-4.50800197027956,336.966494672878));
#51651=CARTESIAN_POINT('Ctrl Pts',(147.219612339209,-4.45390501802296,337.09050678983));
#51652=CARTESIAN_POINT('Ctrl Pts',(147.211978464961,-4.39469775039546,337.212259940699));
#51653=CARTESIAN_POINT('Ctrl Pts',(147.204344590713,-4.33061094379842,337.331306911574));
#51654=CARTESIAN_POINT('Ctrl Pts',(147.196703192206,-4.26646097062505,337.45047122001));
#51655=CARTESIAN_POINT('Ctrl Pts',(147.189061793699,-4.1974220439605,337.566923664982));
#51656=CARTESIAN_POINT('Ctrl Pts',(147.181420395192,-4.12377021101172,337.680242957135));
#51657=CARTESIAN_POINT('Ctrl Pts',(147.173775272607,-4.05008248343362,337.793617476074));
#51658=CARTESIAN_POINT('Ctrl Pts',(147.166130150023,-3.97177760672654,337.903855472973));
#51659=CARTESIAN_POINT('Ctrl Pts',(147.158485027438,-3.88917315145926,338.010567265561));
#51660=CARTESIAN_POINT('Ctrl Pts',(147.150827780779,-3.80643769731258,338.117448287826));
#51661=CARTESIAN_POINT('Ctrl Pts',(147.143170534121,-3.71938930263166,338.220791625409));
#51662=CARTESIAN_POINT('Ctrl Pts',(147.135513287463,-3.62838423958904,338.320242592402));
#51663=CARTESIAN_POINT('Ctrl Pts',(147.128030897298,-3.53945731598285,338.417422554139));
#51664=CARTESIAN_POINT('Ctrl Pts',(147.120548507134,-3.44675278395714,338.510885810321));
#51665=CARTESIAN_POINT('Ctrl Pts',(147.113066116969,-3.3506331052346,338.600338991901));
#51666=CARTESIAN_POINT('Ctrl Pts',(147.105291038191,-3.25075351357949,338.693291313083));
#51667=CARTESIAN_POINT('Ctrl Pts',(147.097515959413,-3.14684517639639,338.782231120297));
#51668=CARTESIAN_POINT('Ctrl Pts',(147.089740880634,-3.03926400149785,338.8667890286));
#51669=CARTESIAN_POINT('Ctrl Pts',(147.081975369585,-2.93181521208375,338.951242883014));
#51670=CARTESIAN_POINT('Ctrl Pts',(147.074209858536,-2.82070288215537,339.031325328226));
#51671=CARTESIAN_POINT('Ctrl Pts',(147.066444347487,-2.70631924063376,339.106704181004));
#51672=CARTESIAN_POINT('Ctrl Pts',(147.058686535965,-2.59204901082594,339.18200829543));
#51673=CARTESIAN_POINT('Ctrl Pts',(147.050928724443,-2.47451424847793,339.252617884604));
#51674=CARTESIAN_POINT('Ctrl Pts',(147.043170912921,-2.35413941223203,339.318241620182));
#51675=CARTESIAN_POINT('Ctrl Pts',(147.035418939398,-2.2338551618677,339.383815971819));
#51676=CARTESIAN_POINT('Ctrl Pts',(147.027666965875,-2.11073543349573,339.444411751719));
#51677=CARTESIAN_POINT('Ctrl Pts',(147.019914992352,-1.98523245490647,339.499781679425));
#51678=CARTESIAN_POINT('Ctrl Pts',(147.012166301794,-1.85978262690325,339.555128157933));
#51679=CARTESIAN_POINT('Ctrl Pts',(147.004417611236,-1.73195191299756,339.605253028605));
#51680=CARTESIAN_POINT('Ctrl Pts',(146.996668920679,-1.602215661884,339.649955702511));
#51681=CARTESIAN_POINT('Ctrl Pts',(146.988921842301,-1.47250640348097,339.694649075653));
#51682=CARTESIAN_POINT('Ctrl Pts',(146.981174763923,-1.34089276578264,339.733922368712));
#51683=CARTESIAN_POINT('Ctrl Pts',(146.973427685545,-1.20786815492982,339.767623892759));
#51684=CARTESIAN_POINT('Ctrl Pts',(146.965680542239,-1.0748424292029,339.801325699258));
#51685=CARTESIAN_POINT('Ctrl Pts',(146.957933398934,-0.9404060856384,339.82945554761));
#51686=CARTESIAN_POINT('Ctrl Pts',(146.950186255628,-0.805065314541873,
339.851912293294));
#51687=CARTESIAN_POINT('Ctrl Pts',(146.9424373706,-0.669694115966915,339.874374087732));
#51688=CARTESIAN_POINT('Ctrl Pts',(146.934688485572,-0.533418470773759,
339.891160177561));
#51689=CARTESIAN_POINT('Ctrl Pts',(146.926939600544,-0.396751932446336,
339.902221023842));
#51690=CARTESIAN_POINT('Ctrl Pts',(146.919182490769,-0.259940334842683,
339.91329361022));
#51691=CARTESIAN_POINT('Ctrl Pts',(146.911425380994,-0.122737405522813,
339.918628782426));
#51692=CARTESIAN_POINT('Ctrl Pts',(146.90366827122,0.0143404839101443,339.918229093182));
#51693=CARTESIAN_POINT('Ctrl Pts',(146.895907016293,0.1514916233845,339.917829190357));
#51694=CARTESIAN_POINT('Ctrl Pts',(146.888145761367,0.288517199548139,339.911688337227));
#51695=CARTESIAN_POINT('Ctrl Pts',(146.880384506441,0.424904702899062,339.899861126191));
#51696=CARTESIAN_POINT('Ctrl Pts',(146.872610836036,0.561510381806624,339.888014995471));
#51697=CARTESIAN_POINT('Ctrl Pts',(146.864837165632,0.697475560361569,339.870464379769));
#51698=CARTESIAN_POINT('Ctrl Pts',(146.857063495227,0.832295792667097,339.847315419488));
#51699=CARTESIAN_POINT('Ctrl Pts',(146.84965169105,0.960840110722838,339.825244048878));
#51700=CARTESIAN_POINT('Ctrl Pts',(146.842239886873,1.08834339670137,339.798083870115));
#51701=CARTESIAN_POINT('Ctrl Pts',(146.834828082696,1.2143820356245,339.76596887674));
#51702=CARTESIAN_POINT('Ctrl Pts',(146.827053003917,1.34659820369113,339.732279831874));
#51703=CARTESIAN_POINT('Ctrl Pts',(146.819277925139,1.47762034853376,339.693031527398));
#51704=CARTESIAN_POINT('Ctrl Pts',(146.81150284636,1.60694524433394,339.648323358396));
#51705=CARTESIAN_POINT('Ctrl Pts',(146.803737335311,1.73611099761656,339.603670205643));
#51706=CARTESIAN_POINT('Ctrl Pts',(146.795971824262,1.86358329162759,339.553570683163));
#51707=CARTESIAN_POINT('Ctrl Pts',(146.788206313213,1.9888705288252,339.498174861215));
#51708=CARTESIAN_POINT('Ctrl Pts',(146.780448501691,2.11403354336215,339.442833964387));
#51709=CARTESIAN_POINT('Ctrl Pts',(146.772690690169,2.23701545733739,339.382207375514));
#51710=CARTESIAN_POINT('Ctrl Pts',(146.764932878647,2.35734158760555,339.316494376441));
#51711=CARTESIAN_POINT('Ctrl Pts',(146.757180905124,2.4775771686453,339.250830828484));
#51712=CARTESIAN_POINT('Ctrl Pts',(146.749428931601,2.59516060234791,339.18008867574));
#51713=CARTESIAN_POINT('Ctrl Pts',(146.741676958078,2.70963921889573,339.104514388563));
#51714=CARTESIAN_POINT('Ctrl Pts',(146.73392826752,2.82406935368132,339.028972107142));
#51715=CARTESIAN_POINT('Ctrl Pts',(146.726179576962,2.93539696101511,338.948601976354));
#51716=CARTESIAN_POINT('Ctrl Pts',(146.718430886405,3.0431961229348,338.863695176881));
#51717=CARTESIAN_POINT('Ctrl Pts',(146.710683808027,3.15097285633847,338.778806042977));
#51718=CARTESIAN_POINT('Ctrl Pts',(146.702936729649,3.25522229767815,338.689382359558));
#51719=CARTESIAN_POINT('Ctrl Pts',(146.695189651271,3.35554987812313,338.595756954791));
#51720=CARTESIAN_POINT('Ctrl Pts',(146.687442507965,3.4558782994101,338.502130765353));
#51721=CARTESIAN_POINT('Ctrl Pts',(146.679695364659,3.55228450847258,338.40430305101));
#51722=CARTESIAN_POINT('Ctrl Pts',(146.671948221354,3.64440952210466,338.302644742883));
#51723=CARTESIAN_POINT('Ctrl Pts',(146.664199336325,3.73655524739532,338.200963579811));
#51724=CARTESIAN_POINT('Ctrl Pts',(146.656450451297,3.82441759955697,338.095450398846));
#51725=CARTESIAN_POINT('Ctrl Pts',(146.648701566269,3.90767700698123,337.986510249708));
#51726=CARTESIAN_POINT('Ctrl Pts',(146.640944456495,3.99102478680095,337.877454470369));
#51727=CARTESIAN_POINT('Ctrl Pts',(146.63318734672,4.06975962468716,337.764964767821));
#51728=CARTESIAN_POINT('Ctrl Pts',(146.625430236945,4.14360422897478,337.649476751384));
#51729=CARTESIAN_POINT('Ctrl Pts',(146.617668982019,4.21748829345771,337.533927021844));
#51730=CARTESIAN_POINT('Ctrl Pts',(146.609907727093,4.28647672083974,337.415376123545));
#51731=CARTESIAN_POINT('Ctrl Pts',(146.602146472166,4.35033807073274,337.29428457974));
#51732=CARTESIAN_POINT('Ctrl Pts',(146.594372801762,4.41430157797325,337.172999328929));
#51733=CARTESIAN_POINT('Ctrl Pts',(146.586599131357,4.47312145060014,337.049165664382));
#51734=CARTESIAN_POINT('Ctrl Pts',(146.578825460952,4.52661395972237,336.923265224078));
#51735=CARTESIAN_POINT('Ctrl Pts',(146.571413656775,4.57761637967503,336.80322547956));
#51736=CARTESIAN_POINT('Ctrl Pts',(146.564001852598,4.623776150096,336.681307315039));
#51737=CARTESIAN_POINT('Ctrl Pts',(146.556590048421,4.6649767066401,336.55793946898));
#51738=CARTESIAN_POINT('Ctrl Pts',(146.548814969643,4.70819662519083,336.42852499729));
#51739=CARTESIAN_POINT('Ctrl Pts',(146.541039890864,4.74609548925451,336.297106170838));
#51740=CARTESIAN_POINT('Ctrl Pts',(146.533264812086,4.77848455791275,336.164159951334));
#51741=CARTESIAN_POINT('Ctrl Pts',(146.525499301037,4.81083376975999,336.031377330616));
#51742=CARTESIAN_POINT('Ctrl Pts',(146.517733789988,4.8376865851279,335.897071432756));
#51743=CARTESIAN_POINT('Ctrl Pts',(146.509968278939,4.85890316966208,335.761736864244));
#51744=CARTESIAN_POINT('Ctrl Pts',(146.502210467417,4.88009871789099,335.626536480349));
#51745=CARTESIAN_POINT('Ctrl Pts',(146.494452655895,4.89566909624876,335.490309839191));
#51746=CARTESIAN_POINT('Ctrl Pts',(146.486694844372,4.90552500680314,335.353563954793));
#51747=CARTESIAN_POINT('Ctrl Pts',(146.478942870849,4.91537350047228,335.21692097601));
#51748=CARTESIAN_POINT('Ctrl Pts',(146.471190897326,4.91951605792517,335.079759920044));
#51749=CARTESIAN_POINT('Ctrl Pts',(146.463438923803,4.91791497572711,334.942594825851));
#51750=CARTESIAN_POINT('Ctrl Pts',(146.455690233246,4.91631457158831,334.805487821158));
#51751=CARTESIAN_POINT('Ctrl Pts',(146.447941542688,4.90897537029277,334.668377171675));
#51752=CARTESIAN_POINT('Ctrl Pts',(146.440192852131,4.89591174323791,334.531778615477));
#51753=CARTESIAN_POINT('Ctrl Pts',(146.432445773753,4.88285083417977,334.395208479749));
#51754=CARTESIAN_POINT('Ctrl Pts',(146.424698695375,4.86406790556275,334.259150614234));
#51755=CARTESIAN_POINT('Ctrl Pts',(146.416951616997,4.83962931585833,334.124116932699));
#51756=CARTESIAN_POINT('Ctrl Pts',(146.409204473691,4.81519052133499,333.989082119452));
#51757=CARTESIAN_POINT('Ctrl Pts',(146.401457330386,4.78509604079177,333.855071891931));
#51758=CARTESIAN_POINT('Ctrl Pts',(146.39371018708,4.74946353171188,333.722588858887));
#51759=CARTESIAN_POINT('Ctrl Pts',(146.385961302052,4.71382301168763,333.590076040846));
#51760=CARTESIAN_POINT('Ctrl Pts',(146.378212417024,4.67264208708522,333.459091477888));
#51761=CARTESIAN_POINT('Ctrl Pts',(146.370463531996,4.62608843431994,333.33012310024));
#51762=CARTESIAN_POINT('Ctrl Pts',(146.362706422221,4.57948536902639,333.201017834224));
#51763=CARTESIAN_POINT('Ctrl Pts',(146.354949312446,4.52749831687509,333.073933396604));
#51764=CARTESIAN_POINT('Ctrl Pts',(146.347192202672,4.47034353260724,332.949338701058));
#51765=CARTESIAN_POINT('Ctrl Pts',(146.339430947746,4.41315820665017,332.824677426091));
#51766=CARTESIAN_POINT('Ctrl Pts',(146.331669692819,4.35079982371003,332.702508892184));
#51767=CARTESIAN_POINT('Ctrl Pts',(146.323908437893,4.2835304019407,332.583276938052));
#51768=CARTESIAN_POINT('Ctrl Pts',(146.316134767489,4.21615337101961,332.463854251652));
#51769=CARTESIAN_POINT('Ctrl Pts',(146.308361097084,4.1438498087889,332.347377864433));
#51770=CARTESIAN_POINT('Ctrl Pts',(146.300587426679,4.06692530865479,332.234262919885));
#51771=CARTESIAN_POINT('Ctrl Pts',(146.293175622502,3.99358166250822,332.126413503219));
#51772=CARTESIAN_POINT('Ctrl Pts',(146.285763818325,3.91603777737317,332.021619853009));
#51773=CARTESIAN_POINT('Ctrl Pts',(146.278352014148,3.83459110891659,331.920212005686));
#51774=CARTESIAN_POINT('Ctrl Pts',(146.27057693537,3.74915249662236,331.813833857688));
#51775=CARTESIAN_POINT('Ctrl Pts',(146.262801856591,3.65914885174212,331.710845626556));
#51776=CARTESIAN_POINT('Ctrl Pts',(146.255026777813,3.56487912301256,331.611664139904));
#51777=CARTESIAN_POINT('Ctrl Pts',(146.247261266764,3.47072539918574,331.512604702386));
#51778=CARTESIAN_POINT('Ctrl Pts',(146.239495755715,3.37231630359424,331.417342969261));
#51779=CARTESIAN_POINT('Ctrl Pts',(146.231730244666,3.26999208899414,331.326264190172));
#51780=CARTESIAN_POINT('Ctrl Pts',(146.223972433143,3.16776932915076,331.235275715957));
#51781=CARTESIAN_POINT('Ctrl Pts',(146.216214621621,3.06163946549021,331.148462200403));
#51782=CARTESIAN_POINT('Ctrl Pts',(146.208456810099,2.95198053268774,331.066173110426));
#51783=CARTESIAN_POINT('Ctrl Pts',(146.200704836576,2.84240412170976,330.9839459456));
#51784=CARTESIAN_POINT('Ctrl Pts',(146.192952863053,2.72930423908257,330.906236662977));
#51785=CARTESIAN_POINT('Ctrl Pts',(146.18520088953,2.61309274763999,330.833355144156));
#51786=CARTESIAN_POINT('Ctrl Pts',(146.177452198972,2.49693047183283,330.760504490701));
#51787=CARTESIAN_POINT('Ctrl Pts',(146.169703508415,2.37765953861018,330.692477741803));
#51788=CARTESIAN_POINT('Ctrl Pts',(146.161954817857,2.25572142030991,330.629541907711));
#51789=CARTESIAN_POINT('Ctrl Pts',(146.154207739479,2.13380867225376,330.566619167945));
#51790=CARTESIAN_POINT('Ctrl Pts',(146.146460661101,2.00923019003613,330.508785415307));
#51791=CARTESIAN_POINT('Ctrl Pts',(146.138713582724,1.88245236324088,330.456261873454));
#51792=CARTESIAN_POINT('Ctrl Pts',(146.130966439418,1.75567347392478,330.403737891403));
#51793=CARTESIAN_POINT('Ctrl Pts',(146.123219296112,1.62669556437602,330.356524358513));
#51794=CARTESIAN_POINT('Ctrl Pts',(146.115472152806,1.49600496023121,330.314794324529));
#51795=CARTESIAN_POINT('Ctrl Pts',(146.107723267778,1.36528497406453,330.273054908748));
#51796=CARTESIAN_POINT('Ctrl Pts',(146.09997438275,1.23285189937561,330.236801563894));
#51797=CARTESIAN_POINT('Ctrl Pts',(146.092225497722,1.09920678643203,330.206157334334));
#51798=CARTESIAN_POINT('Ctrl Pts',(146.084468387947,0.965419821184767,330.175480578672));
#51799=CARTESIAN_POINT('Ctrl Pts',(146.076711278172,0.830418629427339,330.150424918622));
#51800=CARTESIAN_POINT('Ctrl Pts',(146.068954168397,0.694714558523137,330.131062257055));
#51801=CARTESIAN_POINT('Ctrl Pts',(146.061192913471,0.55893797170251,330.1116892487));
#51802=CARTESIAN_POINT('Ctrl Pts',(146.053431658545,0.422458146055808,330.098015339546));
#51803=CARTESIAN_POINT('Ctrl Pts',(146.045670403619,0.285790108086479,330.090060379534));
#51804=CARTESIAN_POINT('Ctrl Pts',(146.037896733214,0.148903445796363,330.082092694178));
#51805=CARTESIAN_POINT('Ctrl Pts',(146.03012306281,0.0118283605679736,330.079862245649));
#51806=CARTESIAN_POINT('Ctrl Pts',(146.022349392405,-0.124920670453566,
330.083336711896));
#51807=CARTESIAN_POINT('Ctrl Pts',(146.014937588228,-0.255304001179753,
330.086649440902));
#51808=CARTESIAN_POINT('Ctrl Pts',(146.007525784051,-0.385390663026766,
330.095147891052));
#51809=CARTESIAN_POINT('Ctrl Pts',(146.000113979874,-0.514742150990681,
330.108760527178));
#51810=CARTESIAN_POINT('Ctrl Pts',(145.992338901095,-0.650433540699215,
330.12304035915));
#51811=CARTESIAN_POINT('Ctrl Pts',(145.984563822317,-0.785744678068278,
330.142993502945));
#51812=CARTESIAN_POINT('Ctrl Pts',(145.976788743539,-0.920163265549295,
330.16859413553));
#51813=CARTESIAN_POINT('Ctrl Pts',(145.96902323249,-1.05441644240055,330.194163264907));
#51814=CARTESIAN_POINT('Ctrl Pts',(145.961257721441,-1.18777887444255,330.225365982945));
#51815=CARTESIAN_POINT('Ctrl Pts',(145.953492210392,-1.31974246674086,330.262124644529));
#51816=CARTESIAN_POINT('Ctrl Pts',(145.945734398869,-1.4515752167533,330.298846859793));
#51817=CARTESIAN_POINT('Ctrl Pts',(145.937976587347,-1.5820115130247,330.341113951702));
#51818=CARTESIAN_POINT('Ctrl Pts',(145.930218775825,-1.71055290511402,330.388797139432));
#51819=CARTESIAN_POINT('Ctrl Pts',(145.922466802302,-1.83899756572923,330.436444444052));
#51820=CARTESIAN_POINT('Ctrl Pts',(145.914714828779,-1.96554979550052,330.489499596449));
#51821=CARTESIAN_POINT('Ctrl Pts',(145.906962855256,-2.08972612576906,330.547783947091));
#51822=CARTESIAN_POINT('Ctrl Pts',(145.899214164699,-2.21384986728844,330.606043614277));
#51823=CARTESIAN_POINT('Ctrl Pts',(145.891465474141,-2.33559935745553,330.669527909354));
#51824=CARTESIAN_POINT('Ctrl Pts',(145.883716783583,-2.45451115564039,330.738010083384));
#51825=CARTESIAN_POINT('Ctrl Pts',(145.875969705206,-2.57339821323243,330.806478009125));
#51826=CARTESIAN_POINT('Ctrl Pts',(145.868222626828,-2.68944841469473,330.879941550535));
#51827=CARTESIAN_POINT('Ctrl Pts',(145.86047554845,-2.80222333816824,330.958128227476));
#51828=CARTESIAN_POINT('Ctrl Pts',(145.852728405144,-2.9149992068047,331.036315559698));
#51829=CARTESIAN_POINT('Ctrl Pts',(145.844981261838,-3.02449942147651,331.119225883701));
#51830=CARTESIAN_POINT('Ctrl Pts',(145.837234118532,-3.13031528225225,331.206543885031));
#51831=CARTESIAN_POINT('Ctrl Pts',(145.829485233504,-3.2361549326792,331.2938815173));
#51832=CARTESIAN_POINT('Ctrl Pts',(145.821736348476,-3.3383082795207,331.385628550024));
#51833=CARTESIAN_POINT('Ctrl Pts',(145.813987463448,-3.43640070509199,331.481430225711));
#51834=CARTESIAN_POINT('Ctrl Pts',(145.806230353673,-3.53459724697764,331.577333586286));
#51835=CARTESIAN_POINT('Ctrl Pts',(145.798473243899,-3.62872397727944,331.677299913212));
#51836=CARTESIAN_POINT('Ctrl Pts',(145.790716134124,-3.71844371193972,331.780938114351));
#51837=CARTESIAN_POINT('Ctrl Pts',(145.782954879198,-3.80821138995743,331.884631696431));
#51838=CARTESIAN_POINT('Ctrl Pts',(145.775193624272,-3.89356713675331,331.992000756635));
#51839=CARTESIAN_POINT('Ctrl Pts',(145.767432369345,-3.9742155496948,332.102622940129));
#51840=CARTESIAN_POINT('Ctrl Pts',(145.759658698941,-4.05499297381374,332.213422083066));
#51841=CARTESIAN_POINT('Ctrl Pts',(145.751885028536,-4.13104779955029,332.327484422921));
#51842=CARTESIAN_POINT('Ctrl Pts',(145.744111358131,-4.20212879410281,332.44435983357));
#51843=CARTESIAN_POINT('Ctrl Pts',(145.736699553954,-4.2699009512586,332.555794665736));
#51844=CARTESIAN_POINT('Ctrl Pts',(145.729287749777,-4.33315178031912,332.669786313979));
#51845=CARTESIAN_POINT('Ctrl Pts',(145.7218759456,-4.39170413651322,332.785927318304));
#51846=CARTESIAN_POINT('Ctrl Pts',(145.713571284239,-4.45730995642682,332.916059157731));
#51847=CARTESIAN_POINT('Ctrl Pts',(145.705266622878,-4.51720247461374,333.049256694741));
#51848=CARTESIAN_POINT('Ctrl Pts',(145.696961961517,-4.5711045508882,333.185010675693));
#51849=CARTESIAN_POINT('Ctrl Pts',(145.688673606317,-4.62490079070571,333.320498104383));
#51850=CARTESIAN_POINT('Ctrl Pts',(145.680385251117,-4.67272992078372,333.458531684975));
#51851=CARTESIAN_POINT('Ctrl Pts',(145.672096895917,-4.71436127248231,333.598578987235));
#51852=CARTESIAN_POINT('Ctrl Pts',(145.663831156675,-4.75587902710266,333.738244150466));
#51853=CARTESIAN_POINT('Ctrl Pts',(145.655565417434,-4.79123264186159,333.879911781521));
#51854=CARTESIAN_POINT('Ctrl Pts',(145.647299678193,-4.82024026447434,334.023031804386));
#51855=CARTESIAN_POINT('Ctrl Pts',(145.639048009204,-4.84919850922091,334.165908202966));
#51856=CARTESIAN_POINT('Ctrl Pts',(145.630796340215,-4.87183222725879,334.310231764971));
#51857=CARTESIAN_POINT('Ctrl Pts',(145.622544671226,-4.88800928385938,334.455437511938));
#51858=CARTESIAN_POINT('Ctrl Pts',(145.614311813416,-4.9041494619198,334.600312236018));
#51859=CARTESIAN_POINT('Ctrl Pts',(145.606078955605,-4.91386229371922,334.746064828373));
#51860=CARTESIAN_POINT('Ctrl Pts',(145.597846097795,-4.91706672384905,334.892120920859));
#51861=CARTESIAN_POINT('Ctrl Pts',(145.595836524046,-4.91784889922728,334.927772027219));
#51862=CARTESIAN_POINT('Ctrl Pts',(145.593826950296,-4.91824353667277,334.963441166378));
#51863=CARTESIAN_POINT('Ctrl Pts',(145.591817376546,-4.91824992125433,334.999119896715));
#51864=CARTESIAN_POINT('',(143.841817376479,-4.91824791238371,335.004531537633));
#51865=CARTESIAN_POINT('Ctrl Pts',(145.591817376508,-4.91824992125445,334.999119897395));
#51866=CARTESIAN_POINT('Ctrl Pts',(145.583803417168,-4.91827538224464,335.141402754277));
#51867=CARTESIAN_POINT('Ctrl Pts',(145.575789457829,-4.91212223074461,335.283602918125));
#51868=CARTESIAN_POINT('Ctrl Pts',(145.567775498489,-4.89983804479466,335.425170786018));
#51869=CARTESIAN_POINT('Ctrl Pts',(145.559754410428,-4.88754293159453,335.566864583908));
#51870=CARTESIAN_POINT('Ctrl Pts',(145.551733322367,-4.8691059386561,335.707924614929));
#51871=CARTESIAN_POINT('Ctrl Pts',(145.543712234306,-4.84462623023812,335.847808794357));
#51872=CARTESIAN_POINT('Ctrl Pts',(145.535372707391,-4.8191746723359,335.993246404623));
#51873=CARTESIAN_POINT('Ctrl Pts',(145.527033180476,-4.78719084347461,336.137412462189));
#51874=CARTESIAN_POINT('Ctrl Pts',(145.518693653561,-4.74884357895388,336.27971392316));
#51875=CARTESIAN_POINT('Ctrl Pts',(145.51064889121,-4.71185171681918,336.416985671003));
#51876=CARTESIAN_POINT('Ctrl Pts',(145.502604128858,-4.66893876593736,336.552522083412));
#51877=CARTESIAN_POINT('Ctrl Pts',(145.494559366506,-4.62030584446402,336.685810477519));
#51878=CARTESIAN_POINT('Ctrl Pts',(145.486505755188,-4.57161942842521,336.819245484342));
#51879=CARTESIAN_POINT('Ctrl Pts',(145.478452143871,-4.51720062509598,336.950427217436));
#51880=CARTESIAN_POINT('Ctrl Pts',(145.470398532553,-4.45729755886688,337.078865443991));
#51881=CARTESIAN_POINT('Ctrl Pts',(145.462330474305,-4.39728703582481,337.20753406881));
#51882=CARTESIAN_POINT('Ctrl Pts',(145.454262416057,-4.33177275744791,337.333449045181));
#51883=CARTESIAN_POINT('Ctrl Pts',(145.44619435781,-4.26104785800794,337.456146211907));
#51884=CARTESIAN_POINT('Ctrl Pts',(145.445342208982,-4.25357788960786,337.4691054945));
#51885=CARTESIAN_POINT('Ctrl Pts',(145.444490060154,-4.24604983198606,337.482028909192));
#51886=CARTESIAN_POINT('Ctrl Pts',(145.443637911326,-4.23846405740514,337.494915929763));
#51887=CARTESIAN_POINT('Ctrl Pts',(145.435862832548,-4.16925080142035,337.612498207501));
#51888=CARTESIAN_POINT('Ctrl Pts',(145.428087753769,-4.09503156604459,337.727383963553));
#51889=CARTESIAN_POINT('Ctrl Pts',(145.420312674991,-4.01604209742396,337.839117633036));
#51890=CARTESIAN_POINT('Ctrl Pts',(145.412547163942,-3.93714983037308,337.950713807126));
#51891=CARTESIAN_POINT('Ctrl Pts',(145.404781652893,-3.85349923332459,338.059165296312));
#51892=CARTESIAN_POINT('Ctrl Pts',(145.397016141844,-3.76537147672452,338.164041830439));
#51893=CARTESIAN_POINT('Ctrl Pts',(145.389258330321,-3.67733109905178,338.268814379177));
#51894=CARTESIAN_POINT('Ctrl Pts',(145.381500518799,-3.58482264576081,338.370018729445));
#51895=CARTESIAN_POINT('Ctrl Pts',(145.373742707277,-3.4881698323431,338.467254574333));
#51896=CARTESIAN_POINT('Ctrl Pts',(145.365990733754,-3.39158975323255,338.564417246163));
#51897=CARTESIAN_POINT('Ctrl Pts',(145.358238760231,-3.29087179618737,338.657617080845));
#51898=CARTESIAN_POINT('Ctrl Pts',(145.350486786708,-3.18637885737033,338.746488067484));
#51899=CARTESIAN_POINT('Ctrl Pts',(145.34273809615,-3.08193017137491,338.835321417209));
#51900=CARTESIAN_POINT('Ctrl Pts',(145.334989405593,-2.97370998045297,338.919829312427));
#51901=CARTESIAN_POINT('Ctrl Pts',(145.327240715035,-2.86211666047963,338.999683898048));
#51902=CARTESIAN_POINT('Ctrl Pts',(145.319493636657,-2.75054655842864,339.079521869256));
#51903=CARTESIAN_POINT('Ctrl Pts',(145.311746558279,-2.63560504094371,339.154708229283));
#51904=CARTESIAN_POINT('Ctrl Pts',(145.303999479902,-2.51772174055153,339.224956839975));
#51905=CARTESIAN_POINT('Ctrl Pts',(145.296252336596,-2.39983745218363,339.295206039419));
#51906=CARTESIAN_POINT('Ctrl Pts',(145.28850519329,-2.27901166750761,339.360517206893));
#51907=CARTESIAN_POINT('Ctrl Pts',(145.280758049984,-2.15570069062842,339.420649001552));
#51908=CARTESIAN_POINT('Ctrl Pts',(145.273009164956,-2.03236199082387,339.480794315115));
#51909=CARTESIAN_POINT('Ctrl Pts',(145.265260279928,-1.90653733827704,339.535757767482));
#51910=CARTESIAN_POINT('Ctrl Pts',(145.2575113949,-1.77870481565397,339.585345378624));
#51911=CARTESIAN_POINT('Ctrl Pts',(145.249754285125,-1.65073661027051,339.634985622569));
#51912=CARTESIAN_POINT('Ctrl Pts',(145.24199717535,-1.52075664258323,339.679238485487));
#51913=CARTESIAN_POINT('Ctrl Pts',(145.234240065576,-1.3892605562768,339.717959110598));
#51914=CARTESIAN_POINT('Ctrl Pts',(145.226478810649,-1.25769420266614,339.756700426773));
#51915=CARTESIAN_POINT('Ctrl Pts',(145.218717555723,-1.12461049516579,339.789903519973));
#51916=CARTESIAN_POINT('Ctrl Pts',(145.210956300797,-0.990516221003158,
339.817474512484));
#51917=CARTESIAN_POINT('Ctrl Pts',(145.203182630392,-0.856207439703273,
339.845089609596));
#51918=CARTESIAN_POINT('Ctrl Pts',(145.195408959988,-0.720885247368624,
339.86705453966));
#51919=CARTESIAN_POINT('Ctrl Pts',(145.187635289583,-0.585063407588459,
339.883327131332));
#51920=CARTESIAN_POINT('Ctrl Pts',(145.180223485406,-0.455564107127322,
339.898842229946));
#51921=CARTESIAN_POINT('Ctrl Pts',(145.172811681229,-0.325610916447216,
339.909182997698));
#51922=CARTESIAN_POINT('Ctrl Pts',(145.165399877052,-0.195648072444255,
339.914357017378));
#51923=CARTESIAN_POINT('Ctrl Pts',(145.157624798274,-0.059315362316982,
339.919784631174));
#51924=CARTESIAN_POINT('Ctrl Pts',(145.149849719495,0.0774588078877579,
339.919543367492));
#51925=CARTESIAN_POINT('Ctrl Pts',(145.142074640717,0.214163768174801,339.913584937996));
#51926=CARTESIAN_POINT('Ctrl Pts',(145.134309129668,0.350700504304823,339.907633840727));
#51927=CARTESIAN_POINT('Ctrl Pts',(145.126543618619,0.487167813204997,339.895979592806));
#51928=CARTESIAN_POINT('Ctrl Pts',(145.11877810757,0.623051714060567,339.878625792588));
#51929=CARTESIAN_POINT('Ctrl Pts',(145.111020296048,0.758800885633423,339.861289198714));
#51930=CARTESIAN_POINT('Ctrl Pts',(145.103262484525,0.893967415083862,339.838264347795));
#51931=CARTESIAN_POINT('Ctrl Pts',(145.095504673003,1.02803949476319,339.809606830055));
#51932=CARTESIAN_POINT('Ctrl Pts',(145.08775269948,1.16201068095075,339.780970878005));
#51933=CARTESIAN_POINT('Ctrl Pts',(145.080000725957,1.29488867601812,339.746710777554));
#51934=CARTESIAN_POINT('Ctrl Pts',(145.072248752434,1.42616930966034,339.706933626331));
#51935=CARTESIAN_POINT('Ctrl Pts',(145.064500061876,1.55739434587615,339.667173320755));
#51936=CARTESIAN_POINT('Ctrl Pts',(145.056751371319,1.68702299284331,339.621900724596));
#51937=CARTESIAN_POINT('Ctrl Pts',(145.049002680761,1.81456396617585,339.571273419427));
#51938=CARTESIAN_POINT('Ctrl Pts',(145.041255602383,1.94207840354359,339.52065664769));
#51939=CARTESIAN_POINT('Ctrl Pts',(145.033508524006,2.06750566817488,339.464687527071));
#51940=CARTESIAN_POINT('Ctrl Pts',(145.025761445628,2.19037264157943,339.403572498951));
#51941=CARTESIAN_POINT('Ctrl Pts',(145.018014302322,2.31324064472761,339.342456958629));
#51942=CARTESIAN_POINT('Ctrl Pts',(145.010267159016,2.43354796387937,339.276195598864));
#51943=CARTESIAN_POINT('Ctrl Pts',(145.00252001571,2.55084471803529,339.205041532134));
#51944=CARTESIAN_POINT('Ctrl Pts',(144.994771130682,2.66816784299142,339.133871468459));
#51945=CARTESIAN_POINT('Ctrl Pts',(144.987022245654,2.78247872199062,339.057806711659));
#51946=CARTESIAN_POINT('Ctrl Pts',(144.979273360626,2.89335551512492,338.977144317924));
#51947=CARTESIAN_POINT('Ctrl Pts',(144.971516250851,3.00434999403337,338.89639630829));
#51948=CARTESIAN_POINT('Ctrl Pts',(144.963759141077,3.11190278931912,338.811041143815));
#51949=CARTESIAN_POINT('Ctrl Pts',(144.956002031302,3.21562386658751,338.721417231531));
#51950=CARTESIAN_POINT('Ctrl Pts',(144.948240776376,3.31940036908317,338.631745427093));
#51951=CARTESIAN_POINT('Ctrl Pts',(144.94047952145,3.4193407889823,338.537800597164));
#51952=CARTESIAN_POINT('Ctrl Pts',(144.932718266523,3.51509193086257,338.439958107315));
#51953=CARTESIAN_POINT('Ctrl Pts',(144.924944596119,3.61099624336468,338.34195910137));
#51954=CARTESIAN_POINT('Ctrl Pts',(144.917170925714,3.70269762471466,338.240050266868));
#51955=CARTESIAN_POINT('Ctrl Pts',(144.909397255309,3.78988258517244,338.13464081724));
#51956=CARTESIAN_POINT('Ctrl Pts',(144.901985451132,3.87300906474586,338.034138202851));
#51957=CARTESIAN_POINT('Ctrl Pts',(144.894573646955,3.95202996514973,337.930453775162));
#51958=CARTESIAN_POINT('Ctrl Pts',(144.887161842778,4.02671126083791,337.823965205937));
#51959=CARTESIAN_POINT('Ctrl Pts',(144.879386764,4.10505290929151,337.712257314721));
#51960=CARTESIAN_POINT('Ctrl Pts',(144.871611685221,4.17886637711192,337.597110435425));
#51961=CARTESIAN_POINT('Ctrl Pts',(144.863836606443,4.24783470477198,337.478927869752));
#51962=CARTESIAN_POINT('Ctrl Pts',(144.856071095394,4.31671816251407,337.360890735251));
#51963=CARTESIAN_POINT('Ctrl Pts',(144.848305584345,4.38076814814295,337.239825681523));
#51964=CARTESIAN_POINT('Ctrl Pts',(144.840540073296,4.4397095430825,337.116166873279));
#51965=CARTESIAN_POINT('Ctrl Pts',(144.832782261774,4.49859249745728,336.992630673103));
#51966=CARTESIAN_POINT('Ctrl Pts',(144.825024450251,4.55237677404497,336.866506186839));
#51967=CARTESIAN_POINT('Ctrl Pts',(144.817266638729,4.60083215136461,336.738253887517));
#51968=CARTESIAN_POINT('Ctrl Pts',(144.809514665206,4.64925106447635,336.610098102118));
#51969=CARTESIAN_POINT('Ctrl Pts',(144.801762691683,4.69234892276857,336.47981805504));
#51970=CARTESIAN_POINT('Ctrl Pts',(144.79401071816,4.72994295144147,336.347895670521));
#51971=CARTESIAN_POINT('Ctrl Pts',(144.786262027602,4.76752105902087,336.21602915521));
#51972=CARTESIAN_POINT('Ctrl Pts',(144.778513337045,4.79959986602726,336.082522060948));
#51973=CARTESIAN_POINT('Ctrl Pts',(144.770764646487,4.82604602399348,335.947872795683));
#51974=CARTESIAN_POINT('Ctrl Pts',(144.763017568109,4.85248667961569,335.813251545323));
#51975=CARTESIAN_POINT('Ctrl Pts',(144.755270489731,4.87329694194463,335.677488979946));
#51976=CARTESIAN_POINT('Ctrl Pts',(144.747523411354,4.88839438038178,335.541094672263));
#51977=CARTESIAN_POINT('Ctrl Pts',(144.739776268048,4.90349194534996,335.404699221465));
#51978=CARTESIAN_POINT('Ctrl Pts',(144.732029124742,4.91287654792509,335.267672406302));
#51979=CARTESIAN_POINT('Ctrl Pts',(144.724281981436,4.9165175793662,335.130529514988));
#51980=CARTESIAN_POINT('Ctrl Pts',(144.716533096408,4.92015942938846,334.993355791042));
#51981=CARTESIAN_POINT('Ctrl Pts',(144.70878421138,4.91805512840861,334.856066329677));
#51982=CARTESIAN_POINT('Ctrl Pts',(144.701035326352,4.91022619553396,334.719176619221));
#51983=CARTESIAN_POINT('Ctrl Pts',(144.693278216577,4.90238895294901,334.582141612611));
#51984=CARTESIAN_POINT('Ctrl Pts',(144.685521106803,4.88881496307622,334.445507595341));
#51985=CARTESIAN_POINT('Ctrl Pts',(144.677763997028,4.869577729618,334.309785687117));
#51986=CARTESIAN_POINT('Ctrl Pts',(144.670002742102,4.85033021639736,334.173991253446));
#51987=CARTESIAN_POINT('Ctrl Pts',(144.662241487176,4.82541350047232,334.039110284189));
#51988=CARTESIAN_POINT('Ctrl Pts',(144.654480232249,4.79495210045156,333.905642920763));
#51989=CARTESIAN_POINT('Ctrl Pts',(144.646706561845,4.76444197211805,333.771962053053));
#51990=CARTESIAN_POINT('Ctrl Pts',(144.63893289144,4.72836953832865,333.639699687236));
#51991=CARTESIAN_POINT('Ctrl Pts',(144.631159221035,4.68690926809982,333.50934089239));
#51992=CARTESIAN_POINT('Ctrl Pts',(144.623747416858,4.64737898342487,333.385050330807));
#51993=CARTESIAN_POINT('Ctrl Pts',(144.616335612681,4.60295127959753,333.262490376587));
#51994=CARTESIAN_POINT('Ctrl Pts',(144.608923808504,4.55381710421111,333.142062206667));
#51995=CARTESIAN_POINT('Ctrl Pts',(144.601148729726,4.50227471652589,333.015731493403));
#51996=CARTESIAN_POINT('Ctrl Pts',(144.593373650947,4.44538995202806,332.891347590057));
#51997=CARTESIAN_POINT('Ctrl Pts',(144.585598572169,4.38333043073824,332.769395284354));
#51998=CARTESIAN_POINT('Ctrl Pts',(144.57783306112,4.3213472776404,332.647593048726));
#51999=CARTESIAN_POINT('Ctrl Pts',(144.570067550071,4.25420221356236,332.528216802081));
#52000=CARTESIAN_POINT('Ctrl Pts',(144.562302039022,4.18211145442319,332.411732848935));
#52001=CARTESIAN_POINT('Ctrl Pts',(144.5545442275,4.1100921734815,332.295364389967));
#52002=CARTESIAN_POINT('Ctrl Pts',(144.546786415977,4.03313716043688,332.181882847809));
#52003=CARTESIAN_POINT('Ctrl Pts',(144.539028604455,3.95150905083111,332.071731008992));
#52004=CARTESIAN_POINT('Ctrl Pts',(144.531276630932,3.86994236896703,331.961662062928));
#52005=CARTESIAN_POINT('Ctrl Pts',(144.523524657409,3.78370982205343,331.854918145497));
#52006=CARTESIAN_POINT('Ctrl Pts',(144.515772683886,3.69311776053167,331.751913752785));
#52007=CARTESIAN_POINT('Ctrl Pts',(144.508023993329,3.60256406480104,331.648952982494));
#52008=CARTESIAN_POINT('Ctrl Pts',(144.500275302771,3.50765478413935,331.54972887997));
#52009=CARTESIAN_POINT('Ctrl Pts',(144.492526612213,3.40873687791834,331.454623297925));
#52010=CARTESIAN_POINT('Ctrl Pts',(144.484779533836,3.30983955239397,331.35953750339));
#52011=CARTESIAN_POINT('Ctrl Pts',(144.477032455458,3.20693554184033,331.26856879565));
#52012=CARTESIAN_POINT('Ctrl Pts',(144.46928537708,3.10040874889419,331.182062251387));
#52013=CARTESIAN_POINT('Ctrl Pts',(144.461538233774,2.99388106315089,331.095554982117));
#52014=CARTESIAN_POINT('Ctrl Pts',(144.453791090468,2.88373083788279,331.013510197317));
#52015=CARTESIAN_POINT('Ctrl Pts',(144.446043947163,2.77037482579719,330.936232488553));
#52016=CARTESIAN_POINT('Ctrl Pts',(144.438295062134,2.65699332887353,330.85893740612));
#52017=CARTESIAN_POINT('Ctrl Pts',(144.430546177106,2.54040493386412,330.786411752494));
#52018=CARTESIAN_POINT('Ctrl Pts',(144.422797292078,2.42105477112437,330.718916392113));
#52019=CARTESIAN_POINT('Ctrl Pts',(144.415040182304,2.3015779288887,330.651349391459));
#52020=CARTESIAN_POINT('Ctrl Pts',(144.407283072529,2.17933380401186,330.588823542329));
#52021=CARTESIAN_POINT('Ctrl Pts',(144.399525962754,2.05479198503054,330.531553630091));
#52022=CARTESIAN_POINT('Ctrl Pts',(144.391764707828,1.93018361488353,330.474253114643));
#52023=CARTESIAN_POINT('Ctrl Pts',(144.384003452902,1.80327546556876,330.422214280706));
#52024=CARTESIAN_POINT('Ctrl Pts',(144.376242197976,1.67455550083665,330.375603073144));
#52025=CARTESIAN_POINT('Ctrl Pts',(144.368468527571,1.54562962611045,330.328917302839));
#52026=CARTESIAN_POINT('Ctrl Pts',(144.360694857166,1.41488651724197,330.287676626628));
#52027=CARTESIAN_POINT('Ctrl Pts',(144.352921186762,1.28282849436297,330.251996828503));
#52028=CARTESIAN_POINT('Ctrl Pts',(144.345509382584,1.15691780421781,330.217977933563));
#52029=CARTESIAN_POINT('Ctrl Pts',(144.338097578407,1.02981214420768,330.189013913817));
#52030=CARTESIAN_POINT('Ctrl Pts',(144.33068577423,0.901952205277398,330.16516129722));
#52031=CARTESIAN_POINT('Ctrl Pts',(144.322910695452,0.76782546986766,330.140139592831));
#52032=CARTESIAN_POINT('Ctrl Pts',(144.315135616673,0.632444781813479,330.120663937634));
#52033=CARTESIAN_POINT('Ctrl Pts',(144.307360537895,0.496308518264394,330.10685572283));
#52034=CARTESIAN_POINT('Ctrl Pts',(144.299595026846,0.360339779054511,330.093064499914));
#52035=CARTESIAN_POINT('Ctrl Pts',(144.291829515797,0.223617699514287,330.084926879907));
#52036=CARTESIAN_POINT('Ctrl Pts',(144.284064004748,0.0866514119003903,
330.082513386361));
#52037=CARTESIAN_POINT('Ctrl Pts',(144.276306193226,-0.0501790732406641,
330.080102285801));
#52038=CARTESIAN_POINT('Ctrl Pts',(144.268548381703,-0.187252896300901,
330.083404024002));
#52039=CARTESIAN_POINT('Ctrl Pts',(144.260790570181,-0.32405558147598,330.092437362334));
#52040=CARTESIAN_POINT('Ctrl Pts',(144.253038596658,-0.460755318292714,
330.101463902793));
#52041=CARTESIAN_POINT('Ctrl Pts',(144.245286623135,-0.597183934901157,
330.116213432497));
#52042=CARTESIAN_POINT('Ctrl Pts',(144.237534649612,-0.732827088897107,
330.136652642441));
#52043=CARTESIAN_POINT('Ctrl Pts',(144.229785959054,-0.868412797936255,
330.157083196367));
#52044=CARTESIAN_POINT('Ctrl Pts',(144.222037268497,-1.00321332026162,330.183198579923));
#52045=CARTESIAN_POINT('Ctrl Pts',(144.214288577939,-1.13671978815685,330.214913669983));
#52046=CARTESIAN_POINT('Ctrl Pts',(144.206541499561,-1.27019847891647,330.246622161454));
#52047=CARTESIAN_POINT('Ctrl Pts',(144.198794421184,-1.40238327072859,330.283927951749));
#52048=CARTESIAN_POINT('Ctrl Pts',(144.191047342806,-1.53277622950449,330.326694949742));
#52049=CARTESIAN_POINT('Ctrl Pts',(144.1833001995,-1.66317028109897,330.369462306164));
#52050=CARTESIAN_POINT('Ctrl Pts',(144.175553056194,-1.79177209829666,330.417690839761));
#52051=CARTESIAN_POINT('Ctrl Pts',(144.167805912888,-1.9181000147502,330.471194926262));
#52052=CARTESIAN_POINT('Ctrl Pts',(144.16005702786,-2.04445633240138,330.524711041618));
#52053=CARTESIAN_POINT('Ctrl Pts',(144.152308142832,-2.1685373721823,330.583504917588));
#52054=CARTESIAN_POINT('Ctrl Pts',(144.144559257804,-2.28988288204651,330.647343403275));
#52055=CARTESIAN_POINT('Ctrl Pts',(144.136802148029,-2.41135718928842,330.711249647791));
#52056=CARTESIAN_POINT('Ctrl Pts',(144.129045038255,-2.53008982009006,330.780211015667));
#52057=CARTESIAN_POINT('Ctrl Pts',(144.12128792848,-2.64564603554945,330.853948852573));
#52058=CARTESIAN_POINT('Ctrl Pts',(144.113526673554,-2.76126400055581,330.927726092621));
#52059=CARTESIAN_POINT('Ctrl Pts',(144.105765418628,-2.87370184779567,331.006284663817));
#52060=CARTESIAN_POINT('Ctrl Pts',(144.098004163701,-2.98255596550833,331.089304029318));
#52061=CARTESIAN_POINT('Ctrl Pts',(144.090230493297,-3.09158421433367,331.172456198748));
#52062=CARTESIAN_POINT('Ctrl Pts',(144.082456822892,-3.19701697703763,331.26008317199));
#52063=CARTESIAN_POINT('Ctrl Pts',(144.074683152487,-3.29848505414383,331.351825194691));
#52064=CARTESIAN_POINT('Ctrl Pts',(144.06727134831,-3.39522976784731,331.439296604163));
#52065=CARTESIAN_POINT('Ctrl Pts',(144.059859544133,-3.48837039592104,331.530508372303));
#52066=CARTESIAN_POINT('Ctrl Pts',(144.052447739957,-3.57762091964424,331.625120503214));
#52067=CARTESIAN_POINT('Ctrl Pts',(144.044765905567,-3.67012305893822,331.723179586202));
#52068=CARTESIAN_POINT('Ctrl Pts',(144.037084071178,-3.75875446931306,331.82521850884));
#52069=CARTESIAN_POINT('Ctrl Pts',(144.029402236789,-3.84314688427203,331.930895067221));
#52070=CARTESIAN_POINT('Ctrl Pts',(144.021586200944,-3.92901363262143,332.038417792448));
#52071=CARTESIAN_POINT('Ctrl Pts',(144.013770165099,-4.01049154587189,332.149706204312));
#52072=CARTESIAN_POINT('Ctrl Pts',(144.005954129254,-4.08723028545093,332.264359004512));
#52073=CARTESIAN_POINT('Ctrl Pts',(143.998291178797,-4.16246601507074,332.376766207489));
#52074=CARTESIAN_POINT('Ctrl Pts',(143.99062822834,-4.23314624883612,332.492406882745));
#52075=CARTESIAN_POINT('Ctrl Pts',(143.982965277882,-4.29898060686261,332.610868608821));
#52076=CARTESIAN_POINT('Ctrl Pts',(143.975307371956,-4.3647716260445,332.729252351386));
#52077=CARTESIAN_POINT('Ctrl Pts',(143.967649466029,-4.42572291897584,332.850453102647));
#52078=CARTESIAN_POINT('Ctrl Pts',(143.959991560102,-4.48158777971099,332.974030100114));
#52079=CARTESIAN_POINT('Ctrl Pts',(143.952336941738,-4.53742865749236,333.097554045601));
#52080=CARTESIAN_POINT('Ctrl Pts',(143.944682323373,-4.58818728196023,333.223451843142));
#52081=CARTESIAN_POINT('Ctrl Pts',(143.937027705009,-4.63366346606154,333.351259284852));
#52082=CARTESIAN_POINT('Ctrl Pts',(143.929093510967,-4.68080061278168,333.483734738782));
#52083=CARTESIAN_POINT('Ctrl Pts',(143.921159316925,-4.72226191421726,333.618261577884));
#52084=CARTESIAN_POINT('Ctrl Pts',(143.913225122884,-4.75787970222818,333.754301881825));
#52085=CARTESIAN_POINT('Ctrl Pts',(143.905569724747,-4.79224593357283,333.885561929641));
#52086=CARTESIAN_POINT('Ctrl Pts',(143.89791432661,-4.82117231235154,334.018230459332));
#52087=CARTESIAN_POINT('Ctrl Pts',(143.890258928474,-4.84455974513305,334.151811378091));
#52088=CARTESIAN_POINT('Ctrl Pts',(143.882601961923,-4.86795196945959,334.285419664496));
#52089=CARTESIAN_POINT('Ctrl Pts',(143.874944995372,-4.88580292996572,334.419940315398));
#52090=CARTESIAN_POINT('Ctrl Pts',(143.867288028821,-4.89806518468095,334.554870233397));
#52091=CARTESIAN_POINT('Ctrl Pts',(143.859625608661,-4.91033617308153,334.689896254067));
#52092=CARTESIAN_POINT('Ctrl Pts',(143.851963188502,-4.91701048961626,334.825331723587));
#52093=CARTESIAN_POINT('Ctrl Pts',(143.844300768342,-4.91809275560886,334.96067176933));
#52094=CARTESIAN_POINT('Ctrl Pts',(143.843472971064,-4.91820967648035,334.975293014203));
#52095=CARTESIAN_POINT('Ctrl Pts',(143.842645173786,-4.91826138136206,334.989913148133));
#52096=CARTESIAN_POINT('Ctrl Pts',(143.841817376508,-4.91824791238418,335.004531537123));
#52097=CARTESIAN_POINT('',(142.091817376456,-4.91824980134024,334.998602102778));
#52098=CARTESIAN_POINT('Ctrl Pts',(143.841817376479,-4.9182479123837,335.004531537634));
#52099=CARTESIAN_POINT('Ctrl Pts',(143.831755391686,-4.91808419516746,335.182219978545));
#52100=CARTESIAN_POINT('Ctrl Pts',(143.821693406893,-4.90828766482633,335.359479490191));
#52101=CARTESIAN_POINT('Ctrl Pts',(143.811631422101,-4.88901797353475,335.535430963761));
#52102=CARTESIAN_POINT('Ctrl Pts',(143.801323074948,-4.86927647407371,335.715690515827));
#52103=CARTESIAN_POINT('Ctrl Pts',(143.791014727794,-4.83959221489103,335.89457752059));
#52104=CARTESIAN_POINT('Ctrl Pts',(143.780706380641,-4.80018467176683,336.071172338811));
#52105=CARTESIAN_POINT('Ctrl Pts',(143.778540822322,-4.79190600869851,336.108271048443));
#52106=CARTESIAN_POINT('Ctrl Pts',(143.776375264002,-4.78319839576932,336.14526867524));
#52107=CARTESIAN_POINT('Ctrl Pts',(143.774209705682,-4.77406413220818,336.182156810268));
#52108=CARTESIAN_POINT('Ctrl Pts',(143.766434626904,-4.74126907047998,336.314597554635));
#52109=CARTESIAN_POINT('Ctrl Pts',(143.758659548125,-4.7029068095277,336.445881859782));
#52110=CARTESIAN_POINT('Ctrl Pts',(143.750884469347,-4.65907334251896,336.575505839891));
#52111=CARTESIAN_POINT('Ctrl Pts',(143.743118958298,-4.61529381538194,336.704970309439));
#52112=CARTESIAN_POINT('Ctrl Pts',(143.735353447249,-4.56605660228122,336.832778152466));
#52113=CARTESIAN_POINT('Ctrl Pts',(143.7275879362,-4.51150844896089,336.958436768817));
#52114=CARTESIAN_POINT('Ctrl Pts',(143.719830124678,-4.45701438029341,337.083970794284));
#52115=CARTESIAN_POINT('Ctrl Pts',(143.712072313155,-4.397220005314,337.207359477575));
#52116=CARTESIAN_POINT('Ctrl Pts',(143.704314501633,-4.33232139449749,337.328126800086));
#52117=CARTESIAN_POINT('Ctrl Pts',(143.69656252811,-4.2674716219436,337.448803241358));
#52118=CARTESIAN_POINT('Ctrl Pts',(143.688810554587,-4.1975254433542,337.566861905406));
#52119=CARTESIAN_POINT('Ctrl Pts',(143.681058581064,-4.12272626535064,337.68184846766));
#52120=CARTESIAN_POINT('Ctrl Pts',(143.673309890507,-4.04795876484348,337.796786333036));
#52121=CARTESIAN_POINT('Ctrl Pts',(143.665561199949,-3.96834256536025,337.90865435732));
#52122=CARTESIAN_POINT('Ctrl Pts',(143.657812509391,-3.88416596355725,338.017024665137));
#52123=CARTESIAN_POINT('Ctrl Pts',(143.650065431014,-3.80000687539927,338.125372425606));
#52124=CARTESIAN_POINT('Ctrl Pts',(143.642318352636,-3.71128951183635,338.230223608614));
#52125=CARTESIAN_POINT('Ctrl Pts',(143.634571274258,-3.61834402784686,338.331181405845));
#52126=CARTESIAN_POINT('Ctrl Pts',(143.626824130952,-3.52539776488478,338.432140049198));
#52127=CARTESIAN_POINT('Ctrl Pts',(143.619076987646,-3.42822357556011,338.529204954125));
#52128=CARTESIAN_POINT('Ctrl Pts',(143.61132984434,-3.32718995734353,338.622014639707));
#52129=CARTESIAN_POINT('Ctrl Pts',(143.603580959312,-3.22613362462457,338.714845190877));
#52130=CARTESIAN_POINT('Ctrl Pts',(143.595832074284,-3.12121642422502,338.803418354673));
#52131=CARTESIAN_POINT('Ctrl Pts',(143.588083189256,-3.01284123768635,338.887411830382));
#52132=CARTESIAN_POINT('Ctrl Pts',(143.580326079481,-2.90435102060488,338.971494457634));
#52133=CARTESIAN_POINT('Ctrl Pts',(143.572568969707,-2.79239579496854,339.050987446816));
#52134=CARTESIAN_POINT('Ctrl Pts',(143.564811859932,-2.67740928685603,339.125610569741));
#52135=CARTESIAN_POINT('Ctrl Pts',(143.557050605006,-2.56236133363025,339.200273568876));
#52136=CARTESIAN_POINT('Ctrl Pts',(143.54928935008,-2.44427920661862,339.270061317661));
#52137=CARTESIAN_POINT('Ctrl Pts',(143.541528095153,-2.32362185501996,339.334739269826));
#52138=CARTESIAN_POINT('Ctrl Pts',(143.533754424749,-2.20277149098079,339.399520685637));
#52139=CARTESIAN_POINT('Ctrl Pts',(143.525980754344,-2.07933802244679,339.459175800561));
#52140=CARTESIAN_POINT('Ctrl Pts',(143.518207083939,-1.95380183518605,339.513517636093));
#52141=CARTESIAN_POINT('Ctrl Pts',(143.510795279762,-1.83410938764405,339.565329846108));
#52142=CARTESIAN_POINT('Ctrl Pts',(143.503383475585,-1.71250584741837,339.612312207165));
#52143=CARTESIAN_POINT('Ctrl Pts',(143.495971671408,-1.58941915571576,339.654345261145));
#52144=CARTESIAN_POINT('Ctrl Pts',(143.48819659263,-1.46029961859701,339.698438480311));
#52145=CARTESIAN_POINT('Ctrl Pts',(143.480421513851,-1.32913982494351,339.73722430726));
#52146=CARTESIAN_POINT('Ctrl Pts',(143.472646435073,-1.19641545050181,339.770510783166));
#52147=CARTESIAN_POINT('Ctrl Pts',(143.464880924024,-1.0638544018525,339.803756297943));
#52148=CARTESIAN_POINT('Ctrl Pts',(143.457115412975,-0.929732978750773,
339.831515832492));
#52149=CARTESIAN_POINT('Ctrl Pts',(143.449349901926,-0.7945448317185,339.853646214228));
#52150=CARTESIAN_POINT('Ctrl Pts',(143.441592090404,-0.659490724127554,
339.875754653626));
#52151=CARTESIAN_POINT('Ctrl Pts',(143.433834278881,-0.523372380664144,
339.892244984619));
#52152=CARTESIAN_POINT('Ctrl Pts',(143.426076467359,-0.386696200512076,
339.903024486071));
#52153=CARTESIAN_POINT('Ctrl Pts',(143.418324493836,-0.250122873519823,
339.913795875606));
#52154=CARTESIAN_POINT('Ctrl Pts',(143.410572520313,-0.112992933505257,
339.918864959115));
#52155=CARTESIAN_POINT('Ctrl Pts',(143.40282054679,0.0241798470182742,339.918190561324));
#52156=CARTESIAN_POINT('Ctrl Pts',(143.395071856232,0.16129453478772,339.917516449141));
#52157=CARTESIAN_POINT('Ctrl Pts',(143.387323165675,0.298451636924919,339.911103695385));
#52158=CARTESIAN_POINT('Ctrl Pts',(143.379574475117,0.435135330035015,339.898963186946));
#52159=CARTESIAN_POINT('Ctrl Pts',(143.371827396739,0.571790584961155,339.886825204442));
#52160=CARTESIAN_POINT('Ctrl Pts',(143.364080318362,0.707972237680056,339.868961872205));
#52161=CARTESIAN_POINT('Ctrl Pts',(143.356333239984,0.843167937808599,339.845436088852));
#52162=CARTESIAN_POINT('Ctrl Pts',(143.348586096678,0.97836477100728,339.82191010833));
#52163=CARTESIAN_POINT('Ctrl Pts',(143.340838953372,1.11257525004651,339.792721649046));
#52164=CARTESIAN_POINT('Ctrl Pts',(143.333091810066,1.24529598278496,339.757984970317));
#52165=CARTESIAN_POINT('Ctrl Pts',(143.325342925038,1.37804655396183,339.723240482045));
#52166=CARTESIAN_POINT('Ctrl Pts',(143.31759404001,1.50930633430796,339.682945391176));
#52167=CARTESIAN_POINT('Ctrl Pts',(143.309845154982,1.63858627195674,339.637264073983));
#52168=CARTESIAN_POINT('Ctrl Pts',(143.302088045207,1.76800342866715,339.591534270168));
#52169=CARTESIAN_POINT('Ctrl Pts',(143.294330935433,1.89543617576038,339.540406950224));
#52170=CARTESIAN_POINT('Ctrl Pts',(143.286573825658,2.02041414930605,339.484095196111));
#52171=CARTESIAN_POINT('Ctrl Pts',(143.278812570732,2.14545890708468,339.427753350797));
#52172=CARTESIAN_POINT('Ctrl Pts',(143.271051315805,2.26804592837122,339.366221726309));
#52173=CARTESIAN_POINT('Ctrl Pts',(143.263290060879,2.38772961445817,339.299759336374));
#52174=CARTESIAN_POINT('Ctrl Pts',(143.255516390475,2.50760475543804,339.233190628276));
#52175=CARTESIAN_POINT('Ctrl Pts',(143.24774272007,2.62456694669851,339.161675596944));
#52176=CARTESIAN_POINT('Ctrl Pts',(143.239969049665,2.73819898972141,339.08551702422));
#52177=CARTESIAN_POINT('Ctrl Pts',(143.232557245488,2.84654143380387,339.012903651378));
#52178=CARTESIAN_POINT('Ctrl Pts',(143.225145441311,2.95185655676719,338.93606949152));
#52179=CARTESIAN_POINT('Ctrl Pts',(143.217733637134,3.05381232018853,338.855309763892));
#52180=CARTESIAN_POINT('Ctrl Pts',(143.209958558356,3.16076523928528,338.770591761444));
#52181=CARTESIAN_POINT('Ctrl Pts',(143.202183479577,3.26435915891964,338.681285929282));
#52182=CARTESIAN_POINT('Ctrl Pts',(143.194408400799,3.36417524137779,338.587688393353));
#52183=CARTESIAN_POINT('Ctrl Pts',(143.18664288975,3.4638684937919,338.494206035151));
#52184=CARTESIAN_POINT('Ctrl Pts',(143.178877378701,3.55979287654325,338.396442746096));
#52185=CARTESIAN_POINT('Ctrl Pts',(143.171111867652,3.65156085012984,338.294736168542));
#52186=CARTESIAN_POINT('Ctrl Pts',(143.163354056129,3.74323783550341,338.193130433356));
#52187=CARTESIAN_POINT('Ctrl Pts',(143.155596244607,3.8307663527579,338.087589478695));
#52188=CARTESIAN_POINT('Ctrl Pts',(143.147838433085,3.91379438905707,337.97848896971));
#52189=CARTESIAN_POINT('Ctrl Pts',(143.140086459562,3.99675994412591,337.869470562318));
#52190=CARTESIAN_POINT('Ctrl Pts',(143.132334486039,4.07523152364888,337.756898242171));
#52191=CARTESIAN_POINT('Ctrl Pts',(143.124582512516,4.14889647067288,337.641181769235));
#52192=CARTESIAN_POINT('Ctrl Pts',(143.116833821958,4.22253022054811,337.525514302293));
#52193=CARTESIAN_POINT('Ctrl Pts',(143.109085131401,4.29136117714352,337.406705659966));
#52194=CARTESIAN_POINT('Ctrl Pts',(143.101336440843,4.3551193538416,337.285195500673));
#52195=CARTESIAN_POINT('Ctrl Pts',(143.093589362465,4.41886426511851,337.163710622583));
#52196=CARTESIAN_POINT('Ctrl Pts',(143.085842284088,4.4775383143312,337.039525691432));
#52197=CARTESIAN_POINT('Ctrl Pts',(143.07809520571,4.53091713207614,336.913105591639));
#52198=CARTESIAN_POINT('Ctrl Pts',(143.070348062404,4.58429639718699,336.786684432323));
#52199=CARTESIAN_POINT('Ctrl Pts',(143.062600919098,4.6323801902699,336.658028427091));
#52200=CARTESIAN_POINT('Ctrl Pts',(143.054853775792,4.67499218005093,336.527622721408));
#52201=CARTESIAN_POINT('Ctrl Pts',(143.047104890764,4.71761374991191,336.397187697754));
#52202=CARTESIAN_POINT('Ctrl Pts',(143.039356005736,4.75476094717216,336.265002562355));
#52203=CARTESIAN_POINT('Ctrl Pts',(143.031607120708,4.7863073453195,336.131567522793));
#52204=CARTESIAN_POINT('Ctrl Pts',(143.023850010933,4.81788722713978,335.997990853902));
#52205=CARTESIAN_POINT('Ctrl Pts',(143.016092901159,4.84385434458669,335.863162011706));
#52206=CARTESIAN_POINT('Ctrl Pts',(143.008335791384,4.86413334191449,335.727591846144));
#52207=CARTESIAN_POINT('Ctrl Pts',(143.000574536458,4.88442317569007,335.591949236221));
#52208=CARTESIAN_POINT('Ctrl Pts',(142.992813281531,4.89901879119825,335.455564902048));
#52209=CARTESIAN_POINT('Ctrl Pts',(142.985052026605,4.90789685957971,335.318953724273));
#52210=CARTESIAN_POINT('Ctrl Pts',(142.977278356201,4.91678912997724,335.182124013135));
#52211=CARTESIAN_POINT('Ctrl Pts',(142.969504685796,4.91994556740354,335.04506712424));
#52212=CARTESIAN_POINT('Ctrl Pts',(142.961731015391,4.91739501751266,334.908297741349));
#52213=CARTESIAN_POINT('Ctrl Pts',(142.954319211214,4.91496319633284,334.777895006138));
#52214=CARTESIAN_POINT('Ctrl Pts',(142.946907407037,4.90734376813904,334.647753899798));
#52215=CARTESIAN_POINT('Ctrl Pts',(142.93949560286,4.89460530405207,334.518313400596));
#52216=CARTESIAN_POINT('Ctrl Pts',(142.931720524082,4.88124248989416,334.382528636944));
#52217=CARTESIAN_POINT('Ctrl Pts',(142.923945445303,4.86220392450461,334.247085789694));
#52218=CARTESIAN_POINT('Ctrl Pts',(142.916170366525,4.83751196939024,334.112497319155));
#52219=CARTESIAN_POINT('Ctrl Pts',(142.908404855476,4.8128503992986,333.978074468299));
#52220=CARTESIAN_POINT('Ctrl Pts',(142.900639344427,4.78254935149013,333.844504283022));
#52221=CARTESIAN_POINT('Ctrl Pts',(142.892873833378,4.74668303676358,333.712295371212));
#52222=CARTESIAN_POINT('Ctrl Pts',(142.885116021856,4.7108522835925,333.580217544924));
#52223=CARTESIAN_POINT('Ctrl Pts',(142.877358210334,4.66946734627238,333.44949868092));
#52224=CARTESIAN_POINT('Ctrl Pts',(142.869600398811,4.62265363529868,333.320638088273));
#52225=CARTESIAN_POINT('Ctrl Pts',(142.861848425288,4.57587515312704,333.191874467308));
#52226=CARTESIAN_POINT('Ctrl Pts',(142.854096451765,4.52367616186882,333.06496670014));
#52227=CARTESIAN_POINT('Ctrl Pts',(142.846344478242,4.46623204080221,332.940399451298));
#52228=CARTESIAN_POINT('Ctrl Pts',(142.838595787685,4.408812247355,332.815884956761));
#52229=CARTESIAN_POINT('Ctrl Pts',(142.830847097127,4.34615190548417,332.693709363314));
#52230=CARTESIAN_POINT('Ctrl Pts',(142.82309840657,4.27847462808346,332.574337632863));
#52231=CARTESIAN_POINT('Ctrl Pts',(142.815351328192,4.21081143150557,332.454990738697));
#52232=CARTESIAN_POINT('Ctrl Pts',(142.807604249814,4.13813356827702,332.338446886982));
#52233=CARTESIAN_POINT('Ctrl Pts',(142.799857171436,4.06071055046379,332.225146330371));
#52234=CARTESIAN_POINT('Ctrl Pts',(142.79211002813,3.98328688377115,332.111844824193));
#52235=CARTESIAN_POINT('Ctrl Pts',(142.784362884825,3.90111820370109,332.001786990056));
#52236=CARTESIAN_POINT('Ctrl Pts',(142.776615741519,3.8145170564545,331.895383648739));
#52237=CARTESIAN_POINT('Ctrl Pts',(142.768866856491,3.72789643943142,331.788956385692));
#52238=CARTESIAN_POINT('Ctrl Pts',(142.761117971463,3.6368416189717,331.686185553469));
#52239=CARTESIAN_POINT('Ctrl Pts',(142.753369086435,3.54170481366177,331.587448157847));
#52240=CARTESIAN_POINT('Ctrl Pts',(142.74561197666,3.4464670291637,331.488605961332));
#52241=CARTESIAN_POINT('Ctrl Pts',(142.737854866885,3.34713887655722,331.393806035297));
#52242=CARTESIAN_POINT('Ctrl Pts',(142.73009775711,3.24410916113689,331.303388198211));
#52243=CARTESIAN_POINT('Ctrl Pts',(142.722336502184,3.14102438993088,331.212922044724));
#52244=CARTESIAN_POINT('Ctrl Pts',(142.714575247258,3.03423441873966,331.126842891306));
#52245=CARTESIAN_POINT('Ctrl Pts',(142.706813992332,2.92415959710192,331.045448987157));
#52246=CARTESIAN_POINT('Ctrl Pts',(142.699040321927,2.8139086916229,330.963924879288));
#52247=CARTESIAN_POINT('Ctrl Pts',(142.691266651523,2.70036275917778,330.887101216812));
#52248=CARTESIAN_POINT('Ctrl Pts',(142.683492981118,2.58397021836186,330.815232267722));
#52249=CARTESIAN_POINT('Ctrl Pts',(142.676081176941,2.47299577832311,330.746708835502));
#52250=CARTESIAN_POINT('Ctrl Pts',(142.668669372764,2.35943403576318,330.682689355086));
#52251=CARTESIAN_POINT('Ctrl Pts',(142.661257568587,2.24369124464108,330.623353719888));
#52252=CARTESIAN_POINT('Ctrl Pts',(142.653482489808,2.12227555454633,330.561109868456));
#52253=CARTESIAN_POINT('Ctrl Pts',(142.64570741103,1.998075914582,330.503823907906));
#52254=CARTESIAN_POINT('Ctrl Pts',(142.637932332251,1.87153536465084,330.451754355649));
#52255=CARTESIAN_POINT('Ctrl Pts',(142.630166821202,1.74515053092237,330.39974887829));
#52256=CARTESIAN_POINT('Ctrl Pts',(142.622401310153,1.61643087688516,330.352947184328));
#52257=CARTESIAN_POINT('Ctrl Pts',(142.614635799104,1.48584426148408,330.31156210523));
#52258=CARTESIAN_POINT('Ctrl Pts',(142.606877987582,1.35538712309224,330.270218059559));
#52259=CARTESIAN_POINT('Ctrl Pts',(142.59912017606,1.22306707733535,330.234280058301));
#52260=CARTESIAN_POINT('Ctrl Pts',(142.591362364538,1.08937187067994,330.203912845885));
#52261=CARTESIAN_POINT('Ctrl Pts',(142.583610391015,0.955777273907336,330.173568485759));
#52262=CARTESIAN_POINT('Ctrl Pts',(142.575858417491,0.820809955689621,330.148786656344));
#52263=CARTESIAN_POINT('Ctrl Pts',(142.568106443968,0.68497238856128,330.12968215725));
#52264=CARTESIAN_POINT('Ctrl Pts',(142.560357753411,0.54919234872331,330.110585748923));
#52265=CARTESIAN_POINT('Ctrl Pts',(142.552609062853,0.412543179255915,330.097161943154));
#52266=CARTESIAN_POINT('Ctrl Pts',(142.544860372296,0.275536886312012,330.089474316656));
#52267=CARTESIAN_POINT('Ctrl Pts',(142.537113293918,0.138559098671562,330.081788289633));
#52268=CARTESIAN_POINT('Ctrl Pts',(142.52936621554,0.00122472536296278,
330.079836089889));
#52269=CARTESIAN_POINT('Ctrl Pts',(142.521619137162,-0.135950167323248,
330.083629324949));
#52270=CARTESIAN_POINT('Ctrl Pts',(142.513871993856,-0.273126209666995,
330.0874225918));
#52271=CARTESIAN_POINT('Ctrl Pts',(142.50612485055,-0.41014237799747,330.096961378694));
#52272=CARTESIAN_POINT('Ctrl Pts',(142.498377707244,-0.546484067674328,
330.112205177559));
#52273=CARTESIAN_POINT('Ctrl Pts',(142.490628822216,-0.682856409857596,
330.127452403554));
#52274=CARTESIAN_POINT('Ctrl Pts',(142.482879937188,-0.818553583268342,
330.148407150344));
#52275=CARTESIAN_POINT('Ctrl Pts',(142.47513105216,-0.953067950019553,330.174977249261));
#52276=CARTESIAN_POINT('Ctrl Pts',(142.467373942385,-1.08772509170952,330.201575549957));
#52277=CARTESIAN_POINT('Ctrl Pts',(142.459616832611,-1.22119653480356,330.233801032961));
#52278=CARTESIAN_POINT('Ctrl Pts',(142.451859722836,-1.35298611384692,330.271510638879));
#52279=CARTESIAN_POINT('Ctrl Pts',(142.44409846791,-1.4848461170275,330.309240395604));
#52280=CARTESIAN_POINT('Ctrl Pts',(142.436337212983,-1.61502209457335,330.352459991508));
#52281=CARTESIAN_POINT('Ctrl Pts',(142.428575958057,-1.74303576711506,330.400977345451));
#52282=CARTESIAN_POINT('Ctrl Pts',(142.420802287653,-1.87125421981323,330.449572311348));
#52283=CARTESIAN_POINT('Ctrl Pts',(142.413028617248,-1.99730309586012,330.503481816431));
#52284=CARTESIAN_POINT('Ctrl Pts',(142.405254946843,-2.1207259108454,330.562466374937));
#52285=CARTESIAN_POINT('Ctrl Pts',(142.397843142666,-2.23840336409796,330.618705188052));
#52286=CARTESIAN_POINT('Ctrl Pts',(142.390431338489,-2.35369348604368,330.679557065814));
#52287=CARTESIAN_POINT('Ctrl Pts',(142.383019534312,-2.46622515314727,330.744777731248));
#52288=CARTESIAN_POINT('Ctrl Pts',(142.375244455534,-2.58427233247129,330.813195055778));
#52289=CARTESIAN_POINT('Ctrl Pts',(142.367469376755,-2.69965687059855,330.886636462385));
#52290=CARTESIAN_POINT('Ctrl Pts',(142.359694297977,-2.81192162040989,330.96486928797));
#52291=CARTESIAN_POINT('Ctrl Pts',(142.351928786928,-2.92404822129954,331.043005843082));
#52292=CARTESIAN_POINT('Ctrl Pts',(142.344163275879,-3.03306235495441,331.125921864191));
#52293=CARTESIAN_POINT('Ctrl Pts',(142.33639776483,-3.13853186153162,331.21333909405));
#52294=CARTESIAN_POINT('Ctrl Pts',(142.328639953308,-3.24389679478593,331.300669649471));
#52295=CARTESIAN_POINT('Ctrl Pts',(142.320882141786,-3.34572379602886,331.392492284269));
#52296=CARTESIAN_POINT('Ctrl Pts',(142.313124330263,-3.44361038055605,331.488485994699));
#52297=CARTESIAN_POINT('Ctrl Pts',(142.30537235674,-3.54142330232418,331.584407466817));
#52298=CARTESIAN_POINT('Ctrl Pts',(142.297620383217,-3.63530143168714,331.68449349423));
#52299=CARTESIAN_POINT('Ctrl Pts',(142.289868409694,-3.72487631448255,331.78838366172));
#52300=CARTESIAN_POINT('Ctrl Pts',(142.282119719137,-3.81441326226192,331.892229831662));
#52301=CARTESIAN_POINT('Ctrl Pts',(142.274371028579,-3.89965033344395,331.99987664199));
#52302=CARTESIAN_POINT('Ctrl Pts',(142.266622338022,-3.98025698910588,332.110927940813));
#52303=CARTESIAN_POINT('Ctrl Pts',(142.258875259644,-4.06084687387988,332.221956134486));
#52304=CARTESIAN_POINT('Ctrl Pts',(142.251128181266,-4.13680802993508,332.336387091603));
#52305=CARTESIAN_POINT('Ctrl Pts',(142.243381102888,-4.20785142317407,332.453793122507));
#52306=CARTESIAN_POINT('Ctrl Pts',(142.235633959582,-4.27889541182511,332.571200137387));
#52307=CARTESIAN_POINT('Ctrl Pts',(142.227886816276,-4.34502135309445,332.691581941372));
#52308=CARTESIAN_POINT('Ctrl Pts',(142.220139672971,-4.40598482898517,332.814483871198));
#52309=CARTESIAN_POINT('Ctrl Pts',(142.212390787943,-4.46696201075934,332.937413431987));
#52310=CARTESIAN_POINT('Ctrl Pts',(142.204641902914,-4.52277424396893,333.062863895951));
#52311=CARTESIAN_POINT('Ctrl Pts',(142.196893017886,-4.57322432322255,333.190358501806));
#52312=CARTESIAN_POINT('Ctrl Pts',(142.189135908112,-4.62372795071169,333.317988431753));
#52313=CARTESIAN_POINT('Ctrl Pts',(142.181378798337,-4.6688579110012,333.447666473691));
#52314=CARTESIAN_POINT('Ctrl Pts',(142.173621688562,-4.70846600219053,333.578897973854));
#52315=CARTESIAN_POINT('Ctrl Pts',(142.165860433636,-4.74809525867737,333.710199599935));
#52316=CARTESIAN_POINT('Ctrl Pts',(142.15809917871,-4.78219666937835,333.84305595992));
#52317=CARTESIAN_POINT('Ctrl Pts',(142.150337923784,-4.8106729350113,333.976960912355));
#52318=CARTESIAN_POINT('Ctrl Pts',(142.142564253379,-4.83919475338887,334.111080069075));
#52319=CARTESIAN_POINT('Ctrl Pts',(142.134790582974,-4.86207337996778,334.246250784604));
#52320=CARTESIAN_POINT('Ctrl Pts',(142.12701691257,-4.87926317352832,334.381959591976));
#52321=CARTESIAN_POINT('Ctrl Pts',(142.119605108393,-4.89565277806326,334.511351121717));
#52322=CARTESIAN_POINT('Ctrl Pts',(142.112193304215,-4.90687123616648,334.641231487608));
#52323=CARTESIAN_POINT('Ctrl Pts',(142.104781500038,-4.91292312931696,334.771156411664));
#52324=CARTESIAN_POINT('Ctrl Pts',(142.100460125528,-4.91645162199873,334.846907772819));
#52325=CARTESIAN_POINT('Ctrl Pts',(142.096138751018,-4.91822823969099,334.922741370048));
#52326=CARTESIAN_POINT('Ctrl Pts',(142.091817376508,-4.91824980133998,334.998602101861));
#52327=CARTESIAN_POINT('',(140.34181737656,-4.91824854457842,334.996216317635));
#52328=CARTESIAN_POINT('Ctrl Pts',(142.091817376456,-4.91824980134024,334.998602102778));
#52329=CARTESIAN_POINT('Ctrl Pts',(142.084099485954,-4.91828830999909,335.134087888651));
#52330=CARTESIAN_POINT('Ctrl Pts',(142.076381595451,-4.91272412795323,335.269800248869));
#52331=CARTESIAN_POINT('Ctrl Pts',(142.068663704949,-4.90152721851429,335.405233252169));
#52332=CARTESIAN_POINT('Ctrl Pts',(142.060955124243,-4.89034381547907,335.540502887816));
#52333=CARTESIAN_POINT('Ctrl Pts',(142.053246543537,-4.87354123299007,335.675493444912));
#52334=CARTESIAN_POINT('Ctrl Pts',(142.045537962831,-4.85114141364458,335.809697503592));
#52335=CARTESIAN_POINT('Ctrl Pts',(142.037836769446,-4.82876306059277,335.943772951246));
#52336=CARTESIAN_POINT('Ctrl Pts',(142.030135576062,-4.80079820753371,336.077063010813));
#52337=CARTESIAN_POINT('Ctrl Pts',(142.022434382677,-4.76732068138356,336.209064342106));
#52338=CARTESIAN_POINT('Ctrl Pts',(142.01473866125,-4.73386694214605,336.340971881997));
#52339=CARTESIAN_POINT('Ctrl Pts',(142.007042939823,-4.69490842178153,336.471592132325));
#52340=CARTESIAN_POINT('Ctrl Pts',(141.999347218396,-4.65057012951809,336.600431358395));
#52341=CARTESIAN_POINT('Ctrl Pts',(141.991654256198,-4.60624773433632,336.729224390361));
#52342=CARTESIAN_POINT('Ctrl Pts',(141.983961294,-4.55654953029598,336.856237292492));
#52343=CARTESIAN_POINT('Ctrl Pts',(141.976268331802,-4.50165046563169,336.980991203357));
#52344=CARTESIAN_POINT('Ctrl Pts',(141.968576551801,-4.4467598374387,337.105725942989));
#52345=CARTESIAN_POINT('Ctrl Pts',(141.960884771799,-4.38667009786801,337.228202018312));
#52346=CARTESIAN_POINT('Ctrl Pts',(141.953192991797,-4.32160425576246,337.347960757567));
#52347=CARTESIAN_POINT('Ctrl Pts',(141.945500668206,-4.25653381535751,337.46772796035));
#52348=CARTESIAN_POINT('Ctrl Pts',(141.937808344615,-4.18648676258374,337.58477709614));
#52349=CARTESIAN_POINT('Ctrl Pts',(141.930116021023,-4.11173172203353,337.698674731887));
#52350=CARTESIAN_POINT('Ctrl Pts',(141.922421427981,-4.03695462665031,337.81260597063));
#52351=CARTESIAN_POINT('Ctrl Pts',(141.914726834938,-3.95746699849299,337.923383528075));
#52352=CARTESIAN_POINT('Ctrl Pts',(141.907032241896,-3.87358009018564,338.030603957533));
#52353=CARTESIAN_POINT('Ctrl Pts',(141.899329328923,-3.7896024775064,338.137940321194));
#52354=CARTESIAN_POINT('Ctrl Pts',(141.891626415951,-3.7012163327452,338.241711565036));
#52355=CARTESIAN_POINT('Ctrl Pts',(141.883923502978,-3.60877264417177,338.34154800432));
#52356=CARTESIAN_POINT('Ctrl Pts',(141.87621587781,-3.51627240391097,338.441445517749));
#52357=CARTESIAN_POINT('Ctrl Pts',(141.868508252642,-3.41970995802508,338.53740315405));
#52358=CARTESIAN_POINT('Ctrl Pts',(141.860800627474,-3.31947139594085,338.629089791398));
#52359=CARTESIAN_POINT('Ctrl Pts',(141.853081740675,-3.21908637504751,338.720910392318));
#52360=CARTESIAN_POINT('Ctrl Pts',(141.845362853877,-3.11501481747229,338.808447280764));
#52361=CARTESIAN_POINT('Ctrl Pts',(141.837643967079,-3.00767429655744,338.891410848051));
#52362=CARTESIAN_POINT('Ctrl Pts',(141.833943799974,-2.95621896693819,338.931180710026));
#52363=CARTESIAN_POINT('Ctrl Pts',(141.83024363287,-2.90401286654154,338.969900317586));
#52364=CARTESIAN_POINT('Ctrl Pts',(141.826543465765,-2.8511040643387,339.00754147537));
#52365=CARTESIAN_POINT('Ctrl Pts',(141.818768386987,-2.73992797592005,339.0866360024));
#52366=CARTESIAN_POINT('Ctrl Pts',(141.810993308208,-2.62528238681406,339.161225684943));
#52367=CARTESIAN_POINT('Ctrl Pts',(141.80321822943,-2.50756844823521,339.230990846116));
#52368=CARTESIAN_POINT('Ctrl Pts',(141.795452718381,-2.38999936415181,339.300670156816));
#52369=CARTESIAN_POINT('Ctrl Pts',(141.787687207332,-2.26936977639406,339.365536561453));
#52370=CARTESIAN_POINT('Ctrl Pts',(141.779921696283,-2.14611198114213,339.425312014638));
#52371=CARTESIAN_POINT('Ctrl Pts',(141.77216388476,-2.02297639635301,339.485028200287));
#52372=CARTESIAN_POINT('Ctrl Pts',(141.764406073238,-1.89721813934193,339.539663310216));
#52373=CARTESIAN_POINT('Ctrl Pts',(141.756648261716,-1.76929611732149,339.588984017376));
#52374=CARTESIAN_POINT('Ctrl Pts',(141.748896288193,-1.64147036067944,339.638267609139));
#52375=CARTESIAN_POINT('Ctrl Pts',(141.74114431467,-1.51148444332078,339.68224461841));
#52376=CARTESIAN_POINT('Ctrl Pts',(141.733392341147,-1.37981904371207,339.720729018818));
#52377=CARTESIAN_POINT('Ctrl Pts',(141.725643650589,-1.24820940447816,339.75919712106));
#52378=CARTESIAN_POINT('Ctrl Pts',(141.717894960032,-1.11492207203931,339.792177131502));
#52379=CARTESIAN_POINT('Ctrl Pts',(141.710146269474,-0.980454542108751,
339.819532337619));
#52380=CARTESIAN_POINT('Ctrl Pts',(141.702399191096,-0.846014989270887,
339.846881852258));
#52381=CARTESIAN_POINT('Ctrl Pts',(141.694652112719,-0.710396110145814,
339.868608812485));
#52382=CARTESIAN_POINT('Ctrl Pts',(141.686905034341,-0.574106908938165,
339.884627347056));
#52383=CARTESIAN_POINT('Ctrl Pts',(141.679157891035,-0.437816565495971,
339.900646015878));
#52384=CARTESIAN_POINT('Ctrl Pts',(141.671410747729,-0.300856276967944,
339.910956117993));
#52385=CARTESIAN_POINT('Ctrl Pts',(141.663663604423,-0.163741113026549,
339.91552356422));
#52386=CARTESIAN_POINT('Ctrl Pts',(141.655914719395,-0.0265951226849824,
339.920092037306));
#52387=CARTESIAN_POINT('Ctrl Pts',(141.648165834367,0.110705421775169,339.918915272406));
#52388=CARTESIAN_POINT('Ctrl Pts',(141.640416949339,0.247644898413444,339.912011305646));
#52389=CARTESIAN_POINT('Ctrl Pts',(141.632659839564,0.38472972402698,339.905100010943));
#52390=CARTESIAN_POINT('Ctrl Pts',(141.62490272979,0.521452325263485,339.892449390898));
#52391=CARTESIAN_POINT('Ctrl Pts',(141.617145620015,0.657301097510161,339.874129494557));
#52392=CARTESIAN_POINT('Ctrl Pts',(141.609384365089,0.793222462997171,339.855799808649));
#52393=CARTESIAN_POINT('Ctrl Pts',(141.601623110163,0.928268684415273,339.831794878306));
#52394=CARTESIAN_POINT('Ctrl Pts',(141.593861855236,1.06193879055035,339.802235840484));
#52395=CARTESIAN_POINT('Ctrl Pts',(141.586088184832,1.19582272529216,339.772629517834));
#52396=CARTESIAN_POINT('Ctrl Pts',(141.578314514427,1.32832576784411,339.73745143367));
#52397=CARTESIAN_POINT('Ctrl Pts',(141.570540844022,1.45896168153539,339.696872776041));
#52398=CARTESIAN_POINT('Ctrl Pts',(141.563129039845,1.58351646201547,339.658183064686));
#52399=CARTESIAN_POINT('Ctrl Pts',(141.555717235668,1.70637376017856,339.614584354454));
#52400=CARTESIAN_POINT('Ctrl Pts',(141.548305431491,1.82713111825514,339.566264878345));
#52401=CARTESIAN_POINT('Ctrl Pts',(141.540530352713,1.95380715416844,339.515577120775));
#52402=CARTESIAN_POINT('Ctrl Pts',(141.532755273934,2.07857251614802,339.459533956218));
#52403=CARTESIAN_POINT('Ctrl Pts',(141.524980195156,2.2009412951417,339.398299725785));
#52404=CARTESIAN_POINT('Ctrl Pts',(141.517214684107,2.3231594915624,339.337140847971));
#52405=CARTESIAN_POINT('Ctrl Pts',(141.509449173058,2.44298662674593,339.270803787689));
#52406=CARTESIAN_POINT('Ctrl Pts',(141.501683662009,2.55995494612406,339.199501605705));
#52407=CARTESIAN_POINT('Ctrl Pts',(141.493925850487,2.67680729107278,339.128270120042));
#52408=CARTESIAN_POINT('Ctrl Pts',(141.486168038964,2.79080612947718,339.052083511731));
#52409=CARTESIAN_POINT('Ctrl Pts',(141.478410227442,2.90150691061789,338.971201418984));
#52410=CARTESIAN_POINT('Ctrl Pts',(141.470658253919,3.01212438591053,338.890380192575));
#52411=CARTESIAN_POINT('Ctrl Pts',(141.462906280396,3.11944842968799,338.804870744657));
#52412=CARTESIAN_POINT('Ctrl Pts',(141.455154306873,3.22306248570729,338.714976618463));
#52413=CARTESIAN_POINT('Ctrl Pts',(141.447405616315,3.32663266111236,338.625120562485));
#52414=CARTESIAN_POINT('Ctrl Pts',(141.439656925758,3.42649567909903,338.530883777119));
#52415=CARTESIAN_POINT('Ctrl Pts',(141.4319082352,3.52226735171192,338.432610634133));
#52416=CARTESIAN_POINT('Ctrl Pts',(141.424161156822,3.61801909822841,338.334357937695));
#52417=CARTESIAN_POINT('Ctrl Pts',(141.416414078445,3.70968091991194,338.232070833809));
#52418=CARTESIAN_POINT('Ctrl Pts',(141.408667000067,3.7969051544197,338.12613088511));
#52419=CARTESIAN_POINT('Ctrl Pts',(141.400919856761,3.88413011995038,338.020190048533));
#52420=CARTESIAN_POINT('Ctrl Pts',(141.393172713455,3.96691717567762,337.910596607839));
#52421=CARTESIAN_POINT('Ctrl Pts',(141.385425570149,4.04495892152719,337.79776524849));
#52422=CARTESIAN_POINT('Ctrl Pts',(141.377676685121,4.12301821281847,337.684908522256));
#52423=CARTESIAN_POINT('Ctrl Pts',(141.369927800093,4.19632984901999,337.56881275023));
#52424=CARTESIAN_POINT('Ctrl Pts',(141.362178915065,4.26462996447618,337.449921290285));
#52425=CARTESIAN_POINT('Ctrl Pts',(141.35442180529,4.33300257438036,337.330903637717));
#52426=CARTESIAN_POINT('Ctrl Pts',(141.346664695515,4.3963528427654,337.209084709089));
#52427=CARTESIAN_POINT('Ctrl Pts',(141.338907585741,4.45446281675794,337.084932631195));
#52428=CARTESIAN_POINT('Ctrl Pts',(141.331146330815,4.51260384286263,336.9607142104));
#52429=CARTESIAN_POINT('Ctrl Pts',(141.323385075888,4.56549884417424,336.834160516513));
#52430=CARTESIAN_POINT('Ctrl Pts',(141.315623820962,4.61297858307357,336.705758381074));
#52431=CARTESIAN_POINT('Ctrl Pts',(141.307850150558,4.66053427408147,336.577150844065));
#52432=CARTESIAN_POINT('Ctrl Pts',(141.300076480153,4.70265727196453,336.446689328896));
#52433=CARTESIAN_POINT('Ctrl Pts',(141.292302809748,4.73922840184171,336.314875362031));
#52434=CARTESIAN_POINT('Ctrl Pts',(141.284891005571,4.77409713682437,336.189197367038));
#52435=CARTESIAN_POINT('Ctrl Pts',(141.277479201394,4.80391918483866,336.062290280168));
#52436=CARTESIAN_POINT('Ctrl Pts',(141.270067397217,4.82863504203796,335.934594400424));
#52437=CARTESIAN_POINT('Ctrl Pts',(141.262292318439,4.8545622970235,335.800639765225));
#52438=CARTESIAN_POINT('Ctrl Pts',(141.25451723966,4.87495210072176,335.665393738487));
#52439=CARTESIAN_POINT('Ctrl Pts',(141.246742160882,4.88967969780799,335.529353865901));
#52440=CARTESIAN_POINT('Ctrl Pts',(141.238976649833,4.90438917164842,335.393481399039));
#52441=CARTESIAN_POINT('Ctrl Pts',(141.231211138784,4.91345026094549,335.256817414925));
#52442=CARTESIAN_POINT('Ctrl Pts',(141.223445627735,4.91678900420613,335.11987055776));
#52443=CARTESIAN_POINT('Ctrl Pts',(141.215687816213,4.92012443709311,334.983059483803));
#52444=CARTESIAN_POINT('Ctrl Pts',(141.20793000469,4.91774880550751,334.845966483187));
#52445=CARTESIAN_POINT('Ctrl Pts',(141.200172193168,4.90963987285681,334.709105893228));
#52446=CARTESIAN_POINT('Ctrl Pts',(141.192420219645,4.90153704243507,334.572348295204));
#52447=CARTESIAN_POINT('Ctrl Pts',(141.184668246122,4.88770952175685,334.435823148333));
#52448=CARTESIAN_POINT('Ctrl Pts',(141.176916272599,4.86818714431858,334.30004500831));
#52449=CARTESIAN_POINT('Ctrl Pts',(141.169167582041,4.84867303461875,334.16432437041));
#52450=CARTESIAN_POINT('Ctrl Pts',(141.161418891484,4.8234689205225,334.029350496234));
#52451=CARTESIAN_POINT('Ctrl Pts',(141.153670200926,4.79265648544831,333.895632816953));
#52452=CARTESIAN_POINT('Ctrl Pts',(141.145923122548,4.76185046115863,333.761942958753));
#52453=CARTESIAN_POINT('Ctrl Pts',(141.138176044171,4.72543852456782,333.629509156234));
#52454=CARTESIAN_POINT('Ctrl Pts',(141.130428965793,4.68355339979543,333.498830251516));
#52455=CARTESIAN_POINT('Ctrl Pts',(141.122681822487,4.6416679239854,333.368150251582));
#52456=CARTESIAN_POINT('Ctrl Pts',(141.114934679181,4.59430928780583,333.239225551006));
#52457=CARTESIAN_POINT('Ctrl Pts',(141.107187535875,4.54165985729162,333.112539059168));
#52458=CARTESIAN_POINT('Ctrl Pts',(141.099438650847,4.48899859006762,332.985824085517));
#52459=CARTESIAN_POINT('Ctrl Pts',(141.091689765819,4.43104431154616,332.861348682783));
#52460=CARTESIAN_POINT('Ctrl Pts',(141.083940880791,4.368027057974,332.739574667611));
#52461=CARTESIAN_POINT('Ctrl Pts',(141.076183771016,4.30494291723782,332.617671400241));
#52462=CARTESIAN_POINT('Ctrl Pts',(141.068426661242,4.23678524652287,332.498475595788));
#52463=CARTESIAN_POINT('Ctrl Pts',(141.060669551467,4.16382975683014,332.382423865742));
#52464=CARTESIAN_POINT('Ctrl Pts',(141.052908296541,4.09083528205633,332.266310121363));
#52465=CARTESIAN_POINT('Ctrl Pts',(141.045147041614,4.01303810128669,332.153344120883));
#52466=CARTESIAN_POINT('Ctrl Pts',(141.037385786688,3.93075601736213,332.043931632308));
#52467=CARTESIAN_POINT('Ctrl Pts',(141.029612116284,3.84834230891896,331.934344119408));
#52468=CARTESIAN_POINT('Ctrl Pts',(141.021838445879,3.76142960871022,331.828321780095));
#52469=CARTESIAN_POINT('Ctrl Pts',(141.014064775474,3.67037516867392,331.726236235816));
#52470=CARTESIAN_POINT('Ctrl Pts',(141.006652971297,3.58355933472722,331.628902798184));
#52471=CARTESIAN_POINT('Ctrl Pts',(140.99924116712,3.49297887930251,331.535148095149));
#52472=CARTESIAN_POINT('Ctrl Pts',(140.991829362943,3.39897185827788,331.445260435822));
#52473=CARTESIAN_POINT('Ctrl Pts',(140.984054284164,3.300357273121,331.350967114549));
#52474=CARTESIAN_POINT('Ctrl Pts',(140.976279205386,3.19766009663694,331.260631508139));
#52475=CARTESIAN_POINT('Ctrl Pts',(140.968504126608,3.09123121334857,331.174627776527));
#52476=CARTESIAN_POINT('Ctrl Pts',(140.960738615559,2.98493329757667,331.088729877982));
#52477=CARTESIAN_POINT('Ctrl Pts',(140.95297310451,2.87491311308065,331.0071534911));
#52478=CARTESIAN_POINT('Ctrl Pts',(140.945207593461,2.76155836481314,330.930236068243));
#52479=CARTESIAN_POINT('Ctrl Pts',(140.937449781938,2.6483160081081,330.853394909234));
#52480=CARTESIAN_POINT('Ctrl Pts',(140.929691970416,2.53174598857351,330.781203739487));
#52481=CARTESIAN_POINT('Ctrl Pts',(140.921934158894,2.41226878993646,330.713959595664));
#52482=CARTESIAN_POINT('Ctrl Pts',(140.914182185371,2.29288150168152,330.646766055192));
#52483=CARTESIAN_POINT('Ctrl Pts',(140.906430211848,2.17059172818094,330.584512321546));
#52484=CARTESIAN_POINT('Ctrl Pts',(140.898678238325,2.04584831491121,330.527451762711));
#52485=CARTESIAN_POINT('Ctrl Pts',(140.890929547767,1.92115773055034,330.470415369057));
#52486=CARTESIAN_POINT('Ctrl Pts',(140.88318085721,1.79401592786528,330.418567938191));
#52487=CARTESIAN_POINT('Ctrl Pts',(140.875432166652,1.66489550198094,330.372116463222));
#52488=CARTESIAN_POINT('Ctrl Pts',(140.867685088274,1.53580194067945,330.32567465287));
#52489=CARTESIAN_POINT('Ctrl Pts',(140.859938009896,1.4047309425843,330.284626697571));
#52490=CARTESIAN_POINT('Ctrl Pts',(140.852190931519,1.27217381931185,330.249130938875));
#52491=CARTESIAN_POINT('Ctrl Pts',(140.844443788213,1.13961558508326,330.21363488269));
#52492=CARTESIAN_POINT('Ctrl Pts',(140.836696644907,1.00557157840645,330.183691217026));
#52493=CARTESIAN_POINT('Ctrl Pts',(140.828949501601,0.870546576806936,330.159407916369));
#52494=CARTESIAN_POINT('Ctrl Pts',(140.821200616573,0.735491218720127,330.13511915631));
#52495=CARTESIAN_POINT('Ctrl Pts',(140.813451731545,0.59945481147108,330.116493362703));
#52496=CARTESIAN_POINT('Ctrl Pts',(140.805702846517,0.462950192340578,330.103587008645));
#52497=CARTESIAN_POINT('Ctrl Pts',(140.797945736742,0.326300685797207,330.090666955649));
#52498=CARTESIAN_POINT('Ctrl Pts',(140.790188626967,0.189182364391768,330.08347850579));
#52499=CARTESIAN_POINT('Ctrl Pts',(140.782431517193,0.0521115870834784,
330.082026083336));
#52500=CARTESIAN_POINT('Ctrl Pts',(140.774670262266,-0.0850324364653443,
330.080572884753));
#52501=CARTESIAN_POINT('Ctrl Pts',(140.76690900734,-0.222128474808211,330.084861808945));
#52502=CARTESIAN_POINT('Ctrl Pts',(140.759147752414,-0.358663327620432,
330.094845193073));
#52503=CARTESIAN_POINT('Ctrl Pts',(140.751374082009,-0.49541659170078,330.104844547362));
#52504=CARTESIAN_POINT('Ctrl Pts',(140.743600411605,-0.631606487849166,
330.120556519806));
#52505=CARTESIAN_POINT('Ctrl Pts',(140.7358267412,-0.766727182138997,330.141881795317));
#52506=CARTESIAN_POINT('Ctrl Pts',(140.728414937023,-0.89555797560102,330.162214374123));
#52507=CARTESIAN_POINT('Ctrl Pts',(140.721003132846,-1.02341658748591,330.187649362083));
#52508=CARTESIAN_POINT('Ctrl Pts',(140.713591328669,-1.14987763108054,330.218058501399));
#52509=CARTESIAN_POINT('Ctrl Pts',(140.705816249891,-1.28253690713004,330.249958083217));
#52510=CARTESIAN_POINT('Ctrl Pts',(140.698041171112,-1.41407738074459,330.287432549786));
#52511=CARTESIAN_POINT('Ctrl Pts',(140.690266092334,-1.54399452910135,330.330389314236));
#52512=CARTESIAN_POINT('Ctrl Pts',(140.682500581285,-1.67375180613595,330.373293217652));
#52513=CARTESIAN_POINT('Ctrl Pts',(140.674735070236,-1.80188936500791,330.421665874178));
#52514=CARTESIAN_POINT('Ctrl Pts',(140.666969559187,-1.92791362543145,330.475363869285));
#52515=CARTESIAN_POINT('Ctrl Pts',(140.659211747664,-2.05381293243391,330.529008622673));
#52516=CARTESIAN_POINT('Ctrl Pts',(140.651453936142,-2.17760275356042,330.587968054733));
#52517=CARTESIAN_POINT('Ctrl Pts',(140.64369612462,-2.29880575647429,330.65204931531));
#52518=CARTESIAN_POINT('Ctrl Pts',(140.635944151097,-2.41991755028547,330.716082352706));
#52519=CARTESIAN_POINT('Ctrl Pts',(140.628192177574,-2.53844605646218,330.785229364786));
#52520=CARTESIAN_POINT('Ctrl Pts',(140.620440204051,-2.65393531641671,330.85925001977));
#52521=CARTESIAN_POINT('Ctrl Pts',(140.612691513493,-2.76937566660064,330.933239326962));
#52522=CARTESIAN_POINT('Ctrl Pts',(140.604942822936,-2.88177900216035,331.012097961445));
#52523=CARTESIAN_POINT('Ctrl Pts',(140.597194132378,-2.99071550983518,331.095540523743));
#52524=CARTESIAN_POINT('Ctrl Pts',(140.589447054,-3.09962935235966,331.17896572512));
#52525=CARTESIAN_POINT('Ctrl Pts',(140.581699975622,-3.20507749161174,331.266972719751));
#52526=CARTESIAN_POINT('Ctrl Pts',(140.573952897245,-3.30666089789679,331.359234040917));
#52527=CARTESIAN_POINT('Ctrl Pts',(140.566205753939,-3.40824515554856,331.45149613532));
#52528=CARTESIAN_POINT('Ctrl Pts',(140.558458610633,-3.50596432628149,331.54801236458));
#52529=CARTESIAN_POINT('Ctrl Pts',(140.550711467327,-3.59945444796407,331.648416681696));
#52530=CARTESIAN_POINT('Ctrl Pts',(140.542962582299,-3.69296558821096,331.748843571834));
#52531=CARTESIAN_POINT('Ctrl Pts',(140.535213697271,-3.78224552114894,331.853160003231));
#52532=CARTESIAN_POINT('Ctrl Pts',(140.527464812243,-3.86696923166633,331.960965280908));
#52533=CARTESIAN_POINT('Ctrl Pts',(140.519707702468,-3.95178286880537,332.068884984221));
#52534=CARTESIAN_POINT('Ctrl Pts',(140.511950592694,-4.03203038121057,332.18030062329));
#52535=CARTESIAN_POINT('Ctrl Pts',(140.504193482919,-4.10742861695991,332.294780375075));
#52536=CARTESIAN_POINT('Ctrl Pts',(140.496432227993,-4.18286714311568,332.409321301179));
#52537=CARTESIAN_POINT('Ctrl Pts',(140.488670973067,-4.25345102817896,332.526929267616));
#52538=CARTESIAN_POINT('Ctrl Pts',(140.48090971814,-4.31894263070444,332.647146920187));
#52539=CARTESIAN_POINT('Ctrl Pts',(140.473136047736,-4.38453899845021,332.767556881824));
#52540=CARTESIAN_POINT('Ctrl Pts',(140.465362377331,-4.44502663300238,332.890584520821));
#52541=CARTESIAN_POINT('Ctrl Pts',(140.457588706926,-4.50021531477412,333.015750725546));
#52542=CARTESIAN_POINT('Ctrl Pts',(140.450176902749,-4.55283495013235,333.135090413329));
#52543=CARTESIAN_POINT('Ctrl Pts',(140.442765098572,-4.60063775754223,333.256373779252));
#52544=CARTESIAN_POINT('Ctrl Pts',(140.435353294395,-4.64350139056349,333.379173698901));
#52545=CARTESIAN_POINT('Ctrl Pts',(140.426243114137,-4.69618700043698,333.530112576524));
#52546=CARTESIAN_POINT('Ctrl Pts',(140.417132933879,-4.74154784846308,333.683732773459));
#52547=CARTESIAN_POINT('Ctrl Pts',(140.408022753621,-4.77934383766862,333.839372779985));
#52548=CARTESIAN_POINT('Ctrl Pts',(140.398953508521,-4.8169699965573,333.994313442688));
#52549=CARTESIAN_POINT('Ctrl Pts',(140.389884263422,-4.84709904108127,334.151255712227));
#52550=CARTESIAN_POINT('Ctrl Pts',(140.380815018322,-4.86954082486031,334.30952536794));
#52551=CARTESIAN_POINT('Ctrl Pts',(140.371821738399,-4.89179463333796,334.46646933642));
#52552=CARTESIAN_POINT('Ctrl Pts',(140.362828458477,-4.90648934504363,334.62471843884));
#52553=CARTESIAN_POINT('Ctrl Pts',(140.353835178554,-4.91348676092799,334.783595488297));
#52554=CARTESIAN_POINT('Ctrl Pts',(140.349829244556,-4.91660366448597,334.854365105098));
#52555=CARTESIAN_POINT('Ctrl Pts',(140.345823310558,-4.91819395609712,334.925259061498));
#52556=CARTESIAN_POINT('Ctrl Pts',(140.34181737656,-4.91824854457842,334.996216317635));
#52557=CARTESIAN_POINT('',(138.591817376453,-4.91824901572479,335.003111562653));
#52558=CARTESIAN_POINT('Ctrl Pts',(140.341817376508,-4.91824854457913,334.996216318558));
#52559=CARTESIAN_POINT('Ctrl Pts',(140.334071246083,-4.91835410033541,335.133423811481));
#52560=CARTESIAN_POINT('Ctrl Pts',(140.326325115657,-4.91271371046934,335.270696396518));
#52561=CARTESIAN_POINT('Ctrl Pts',(140.318578985232,-4.90133781675005,335.407517691145));
#52562=CARTESIAN_POINT('Ctrl Pts',(140.310833980913,-4.8899635768191,335.544319095162));
#52563=CARTESIAN_POINT('Ctrl Pts',(140.303088976593,-4.87285552357827,335.680668950269));
#52564=CARTESIAN_POINT('Ctrl Pts',(140.295343972274,-4.85007611703448,335.816054361836));
#52565=CARTESIAN_POINT('Ctrl Pts',(140.287598422206,-4.82729510535177,335.951449313265));
#52566=CARTESIAN_POINT('Ctrl Pts',(140.279852872139,-4.79884200950008,336.085879300777));
#52567=CARTESIAN_POINT('Ctrl Pts',(140.272107322072,-4.76483065272342,336.218840397003));
#52568=CARTESIAN_POINT('Ctrl Pts',(140.264359554399,-4.73080955825472,336.351839560932));
#52569=CARTESIAN_POINT('Ctrl Pts',(140.256611786726,-4.69122713253466,336.483368618452));
#52570=CARTESIAN_POINT('Ctrl Pts',(140.248864019053,-4.64624731565618,336.612937985249));
#52571=CARTESIAN_POINT('Ctrl Pts',(140.241107324421,-4.60121567314095,336.742656641557));
#52572=CARTESIAN_POINT('Ctrl Pts',(140.233350629789,-4.55077434550523,336.87041072746));
#52573=CARTESIAN_POINT('Ctrl Pts',(140.225593935157,-4.49513599603105,336.995729300202));
#52574=CARTESIAN_POINT('Ctrl Pts',(140.21783269349,-4.43946503092494,337.121121335664));
#52575=CARTESIAN_POINT('Ctrl Pts',(140.210071451823,-4.37859114722553,337.244074663837));
#52576=CARTESIAN_POINT('Ctrl Pts',(140.202310210156,-4.31277293739774,337.364143111774));
#52577=CARTESIAN_POINT('Ctrl Pts',(140.194535978122,-4.24684456442897,337.484412524117));
#52578=CARTESIAN_POINT('Ctrl Pts',(140.186761746087,-4.17595553096736,337.601787073513));
#52579=CARTESIAN_POINT('Ctrl Pts',(140.178987514052,-4.10040821333633,337.715848955024));
#52580=CARTESIAN_POINT('Ctrl Pts',(140.171696762742,-4.02955919537855,337.822817310021));
#52581=CARTESIAN_POINT('Ctrl Pts',(140.164406011431,-3.9546138388079,337.926872302788));
#52582=CARTESIAN_POINT('Ctrl Pts',(140.157115260121,-3.87585246189446,338.027697269564));
#52583=CARTESIAN_POINT('Ctrl Pts',(140.149340181342,-3.79185893583497,338.135220078411));
#52584=CARTESIAN_POINT('Ctrl Pts',(140.141565102564,-3.70325499232363,338.239414958504));
#52585=CARTESIAN_POINT('Ctrl Pts',(140.133790023785,-3.61033392100321,338.339861081146));
#52586=CARTESIAN_POINT('Ctrl Pts',(140.126024512736,-3.51752719497677,338.440183598439));
#52587=CARTESIAN_POINT('Ctrl Pts',(140.118259001687,-3.42041417438976,338.536766252812));
#52588=CARTESIAN_POINT('Ctrl Pts',(140.110493490638,-3.31932987578775,338.62921923259));
#52589=CARTESIAN_POINT('Ctrl Pts',(140.102735679116,-3.21834580256201,338.72158054497));
#52590=CARTESIAN_POINT('Ctrl Pts',(140.094977867594,-3.11339857380751,338.809820069109));
#52591=CARTESIAN_POINT('Ctrl Pts',(140.087220056072,-3.00486146800485,338.893583262318));
#52592=CARTESIAN_POINT('Ctrl Pts',(140.079468082549,-2.89640603981643,338.977283421067));
#52593=CARTESIAN_POINT('Ctrl Pts',(140.071716109026,-2.78436641996992,339.056513716034));
#52594=CARTESIAN_POINT('Ctrl Pts',(140.063964135503,-2.66915024685847,339.130958729181));
#52595=CARTESIAN_POINT('Ctrl Pts',(140.056215444945,-2.55398286786457,339.20537221482));
#52596=CARTESIAN_POINT('Ctrl Pts',(140.048466754388,-2.43564193887897,339.275004237657));
#52597=CARTESIAN_POINT('Ctrl Pts',(140.04071806383,-2.31456528433585,339.339581847027));
#52598=CARTESIAN_POINT('Ctrl Pts',(140.032970985452,-2.19351382080196,339.404146020487));
#52599=CARTESIAN_POINT('Ctrl Pts',(140.025223907074,-2.06972810853936,339.46365768838));
#52600=CARTESIAN_POINT('Ctrl Pts',(140.017476828696,-1.94367150558177,339.5178893458));
#52601=CARTESIAN_POINT('Ctrl Pts',(140.009729685391,-1.81761384614856,339.572121457732));
#52602=CARTESIAN_POINT('Ctrl Pts',(140.001982542085,-1.68928561711503,339.621073316455));
#52603=CARTESIAN_POINT('Ctrl Pts',(139.994235398779,-1.55917076163119,339.664565317216));
#52604=CARTESIAN_POINT('Ctrl Pts',(139.986486513751,-1.42902665356533,339.708067095902));
#52605=CARTESIAN_POINT('Ctrl Pts',(139.978737628723,-1.29709549040808,339.746106450163));
#52606=CARTESIAN_POINT('Ctrl Pts',(139.970988743695,-1.16387661422478,339.778553577115));
#52607=CARTESIAN_POINT('Ctrl Pts',(139.96323163392,-1.03051633814994,339.811035143783));
#52608=CARTESIAN_POINT('Ctrl Pts',(139.955474524145,-0.895865999125841,
339.837912533483));
#52609=CARTESIAN_POINT('Ctrl Pts',(139.947717414371,-0.760435926352462,
339.859106941035));
#52610=CARTESIAN_POINT('Ctrl Pts',(139.939956159445,-0.62493348407827,339.8803126742));
#52611=CARTESIAN_POINT('Ctrl Pts',(139.932194904518,-0.488650865980823,
339.895829329916));
#52612=CARTESIAN_POINT('Ctrl Pts',(139.924433649592,-0.352102783357451,
339.90563010147));
#52613=CARTESIAN_POINT('Ctrl Pts',(139.916659979188,-0.21533626830303,339.915446551065));
#52614=CARTESIAN_POINT('Ctrl Pts',(139.908886308783,-0.0783038310392436,
339.919528833328));
#52615=CARTESIAN_POINT('Ctrl Pts',(139.901112638378,0.0584796615429201,
339.9179023162));
#52616=CARTESIAN_POINT('Ctrl Pts',(139.893700834201,0.188895849637867,339.916351513836));
#52617=CARTESIAN_POINT('Ctrl Pts',(139.886289030024,0.319085460811378,339.90961145535));
#52618=CARTESIAN_POINT('Ctrl Pts',(139.878877225847,0.448609063566037,339.897747744687));
#52619=CARTESIAN_POINT('Ctrl Pts',(139.871102147068,0.584481003922257,339.885302558225));
#52620=CARTESIAN_POINT('Ctrl Pts',(139.86332706829,0.720049379420246,339.867179440163));
#52621=CARTESIAN_POINT('Ctrl Pts',(139.855551989512,0.85480159037561,339.843397289464));
#52622=CARTESIAN_POINT('Ctrl Pts',(139.847786478463,0.989387980156876,339.819644404216));
#52623=CARTESIAN_POINT('Ctrl Pts',(139.840020967414,1.12315982250328,339.790246409582));
#52624=CARTESIAN_POINT('Ctrl Pts',(139.832255456365,1.25560801978681,339.755274078657));
#52625=CARTESIAN_POINT('Ctrl Pts',(139.824497644842,1.38792489429724,339.7203364229));
#52626=CARTESIAN_POINT('Ctrl Pts',(139.81673983332,1.51892036000345,339.679835528984));
#52627=CARTESIAN_POINT('Ctrl Pts',(139.808982021798,1.64809427199002,339.633893431353));
#52628=CARTESIAN_POINT('Ctrl Pts',(139.801230048275,1.77717097651059,339.587985906607));
#52629=CARTESIAN_POINT('Ctrl Pts',(139.793478074752,1.90442848898363,339.536645458858));
#52630=CARTESIAN_POINT('Ctrl Pts',(139.785726101229,2.02938097112651,339.480044189127));
#52631=CARTESIAN_POINT('Ctrl Pts',(139.777977410671,2.15428053581937,339.423466890067));
#52632=CARTESIAN_POINT('Ctrl Pts',(139.770228720114,2.27687665643151,339.361633361231));
#52633=CARTESIAN_POINT('Ctrl Pts',(139.762480029556,2.39670287100438,339.294764069261));
#52634=CARTESIAN_POINT('Ctrl Pts',(139.754732951178,2.51650415473262,339.227908690006));
#52635=CARTESIAN_POINT('Ctrl Pts',(139.7469858728,2.63353633761827,339.156019821988));
#52636=CARTESIAN_POINT('Ctrl Pts',(139.739238794422,2.74735735631053,339.079363996903));
#52637=CARTESIAN_POINT('Ctrl Pts',(139.731491651117,2.8611793289324,339.002707529368));
#52638=CARTESIAN_POINT('Ctrl Pts',(139.723744507811,2.97178975947713,338.921284243423));
#52639=CARTESIAN_POINT('Ctrl Pts',(139.715997364505,3.07877572506905,338.835403902749));
#52640=CARTESIAN_POINT('Ctrl Pts',(139.708248479477,3.18578574337701,338.749504254353));
#52641=CARTESIAN_POINT('Ctrl Pts',(139.700499594449,3.28916937050212,338.659145801915));
#52642=CARTESIAN_POINT('Ctrl Pts',(139.692750709421,3.38854722978495,338.564678209042));
#52643=CARTESIAN_POINT('Ctrl Pts',(139.684993599646,3.4880305697548,338.470110347289));
#52644=CARTESIAN_POINT('Ctrl Pts',(139.677236489871,3.58349936483849,338.371424902356));
#52645=CARTESIAN_POINT('Ctrl Pts',(139.669479380097,3.67461117766518,338.269008374948));
#52646=CARTESIAN_POINT('Ctrl Pts',(139.66171812517,3.76577167773145,338.166537119422));
#52647=CARTESIAN_POINT('Ctrl Pts',(139.653956870244,3.85257030910377,338.060331111155));
#52648=CARTESIAN_POINT('Ctrl Pts',(139.646195615318,3.93470598962873,337.950808675207));
#52649=CARTESIAN_POINT('Ctrl Pts',(139.638421944913,4.01697306047458,337.841111039056));
#52650=CARTESIAN_POINT('Ctrl Pts',(139.630648274509,4.09456205344434,337.728086696275));
#52651=CARTESIAN_POINT('Ctrl Pts',(139.622874604104,4.16721567696262,337.612182337467));
#52652=CARTESIAN_POINT('Ctrl Pts',(139.615462799927,4.23648725682591,337.501673354448));
#52653=CARTESIAN_POINT('Ctrl Pts',(139.60805099575,4.30127246673542,337.388546700549));
#52654=CARTESIAN_POINT('Ctrl Pts',(139.600639191573,4.36138867285053,337.273207405151));
#52655=CARTESIAN_POINT('Ctrl Pts',(139.592864112795,4.42445135330487,337.152214987305));
#52656=CARTESIAN_POINT('Ctrl Pts',(139.585089034016,4.4825750635807,337.028405189037));
#52657=CARTESIAN_POINT('Ctrl Pts',(139.577313955238,4.53549829911642,336.90221929367));
#52658=CARTESIAN_POINT('Ctrl Pts',(139.569548444189,4.58835640924168,336.776188678081));
#52659=CARTESIAN_POINT('Ctrl Pts',(139.56178293314,4.63602662809492,336.647788140201));
#52660=CARTESIAN_POINT('Ctrl Pts',(139.554017422091,4.67829296834463,336.517484090473));
#52661=CARTESIAN_POINT('Ctrl Pts',(139.546259610569,4.72051740139483,336.387309237589));
#52662=CARTESIAN_POINT('Ctrl Pts',(139.538501799046,4.75734849866355,336.255234998172));
#52663=CARTESIAN_POINT('Ctrl Pts',(139.530743987524,4.78861822440726,336.121747994594));
#52664=CARTESIAN_POINT('Ctrl Pts',(139.522992014001,4.81986441869061,335.988361444219));
#52665=CARTESIAN_POINT('Ctrl Pts',(139.515240040478,4.84555748291161,335.853564624869));
#52666=CARTESIAN_POINT('Ctrl Pts',(139.507488066955,4.8655792255192,335.71785922206));
#52667=CARTESIAN_POINT('Ctrl Pts',(139.499739376398,4.885592488907,335.582211290568));
#52668=CARTESIAN_POINT('Ctrl Pts',(139.49199068584,4.89993915077576,335.445655926812));
#52669=CARTESIAN_POINT('Ctrl Pts',(139.484241995282,4.90855217689696,335.308704695753));
#52670=CARTESIAN_POINT('Ctrl Pts',(139.476494916905,4.91716341100615,335.171781958542));
#52671=CARTESIAN_POINT('Ctrl Pts',(139.468747838527,4.92004335767285,335.034463907715));
#52672=CARTESIAN_POINT('Ctrl Pts',(139.461000760149,4.91717692324133,334.897266519367));
#52673=CARTESIAN_POINT('Ctrl Pts',(139.453253616843,4.91431046478634,334.760067981174));
#52674=CARTESIAN_POINT('Ctrl Pts',(139.445506473537,4.90569753733867,334.622990498267));
#52675=CARTESIAN_POINT('Ctrl Pts',(139.437759330231,4.89137517152524,334.486548937204));
#52676=CARTESIAN_POINT('Ctrl Pts',(139.430010445203,4.87704958573992,334.350076701182));
#52677=CARTESIAN_POINT('Ctrl Pts',(139.422261560175,4.85701204816055,334.214241060158));
#52678=CARTESIAN_POINT('Ctrl Pts',(139.414512675147,4.83135129589439,334.0795502631));
#52679=CARTESIAN_POINT('Ctrl Pts',(139.406755565372,4.80566330704062,333.944716503838));
#52680=CARTESIAN_POINT('Ctrl Pts',(139.398998455598,4.77434025405274,333.811030400492));
#52681=CARTESIAN_POINT('Ctrl Pts',(139.391241345823,4.73752184110986,333.678989073661));
#52682=CARTESIAN_POINT('Ctrl Pts',(139.383480090897,4.70068375358436,333.546877188167));
#52683=CARTESIAN_POINT('Ctrl Pts',(139.375718835971,4.65834457536707,333.416412202106));
#52684=CARTESIAN_POINT('Ctrl Pts',(139.367957581045,4.61069315209675,333.288073681577));
#52685=CARTESIAN_POINT('Ctrl Pts',(139.36018391064,4.5629655020787,333.159529861241));
#52686=CARTESIAN_POINT('Ctrl Pts',(139.352410240235,4.50990877711769,333.03311966455));
#52687=CARTESIAN_POINT('Ctrl Pts',(139.344636569831,4.45175937363502,332.909301183395));
#52688=CARTESIAN_POINT('Ctrl Pts',(139.337224765653,4.39631683887354,332.791246482325));
#52689=CARTESIAN_POINT('Ctrl Pts',(139.329812961476,4.33624521661356,332.675547893546));
#52690=CARTESIAN_POINT('Ctrl Pts',(139.322401157299,4.27178627105111,332.56257818239));
#52691=CARTESIAN_POINT('Ctrl Pts',(139.31462607852,4.20416800055442,332.444071489173));
#52692=CARTESIAN_POINT('Ctrl Pts',(139.306850999742,4.13150777459266,332.32819343514));
#52693=CARTESIAN_POINT('Ctrl Pts',(139.299075920964,4.05403516260341,332.215402728782));
#52694=CARTESIAN_POINT('Ctrl Pts',(139.291310409915,3.97665788559533,332.102750818569));
#52695=CARTESIAN_POINT('Ctrl Pts',(139.283544898866,3.89448022472525,331.993179015868));
#52696=CARTESIAN_POINT('Ctrl Pts',(139.275779387817,3.80777751134433,331.887121350486));
#52697=CARTESIAN_POINT('Ctrl Pts',(139.268021576294,3.72116076395599,331.781168841588));
#52698=CARTESIAN_POINT('Ctrl Pts',(139.260263764772,3.63002813845001,331.678723836771));
#52699=CARTESIAN_POINT('Ctrl Pts',(139.25250595325,3.53469791217641,331.580190980163));
#52700=CARTESIAN_POINT('Ctrl Pts',(139.244753979727,3.43943942492125,331.481732272655));
#52701=CARTESIAN_POINT('Ctrl Pts',(139.237002006204,3.33998989508302,331.387180133224));
#52702=CARTESIAN_POINT('Ctrl Pts',(139.229250032681,3.23670724048409,331.296905442485));
#52703=CARTESIAN_POINT('Ctrl Pts',(139.221501342123,3.13346832615099,331.206668983131));
#52704=CARTESIAN_POINT('Ctrl Pts',(139.213752651566,3.02639980943565,331.12070662622));
#52705=CARTESIAN_POINT('Ctrl Pts',(139.206003961008,2.91589560016169,331.039351579418));
#52706=CARTESIAN_POINT('Ctrl Pts',(139.19825688263,2.80541438221152,330.958013459214));
#52707=CARTESIAN_POINT('Ctrl Pts',(139.190509804252,2.69149920811127,330.88128097401));
#52708=CARTESIAN_POINT('Ctrl Pts',(139.182762725875,2.57457580512539,330.809446040657));
#52709=CARTESIAN_POINT('Ctrl Pts',(139.175015582569,2.45765142220858,330.737610505259));
#52710=CARTESIAN_POINT('Ctrl Pts',(139.167268439263,2.33771909316038,330.670672808193));
#52711=CARTESIAN_POINT('Ctrl Pts',(139.159521295957,2.21523181965056,330.608880433453));
#52712=CARTESIAN_POINT('Ctrl Pts',(139.151772410929,2.09271700840138,330.547074166477));
#52713=CARTESIAN_POINT('Ctrl Pts',(139.144023525901,1.96764645860009,330.490415699704));
#52714=CARTESIAN_POINT('Ctrl Pts',(139.136274640873,1.84049558838708,330.439105454889));
#52715=CARTESIAN_POINT('Ctrl Pts',(139.128517531098,1.71320975892637,330.387740748849));
#52716=CARTESIAN_POINT('Ctrl Pts',(139.120760421323,1.58383956126605,330.341735750927));
#52717=CARTESIAN_POINT('Ctrl Pts',(139.113003311549,1.45287863667205,330.301242001379));
#52718=CARTESIAN_POINT('Ctrl Pts',(139.105242056622,1.32184773074736,330.260726613267));
#52719=CARTESIAN_POINT('Ctrl Pts',(139.097480801696,1.18922478186493,330.225728441459));
#52720=CARTESIAN_POINT('Ctrl Pts',(139.08971954677,1.05551526260032,330.196348202365));
#52721=CARTESIAN_POINT('Ctrl Pts',(139.081945876365,0.92159185168082,330.166920964464));
#52722=CARTESIAN_POINT('Ctrl Pts',(139.074172205961,0.786578782169621,330.143129685555));
#52723=CARTESIAN_POINT('Ctrl Pts',(139.066398535556,0.650989200978109,330.12502347465));
#52724=CARTESIAN_POINT('Ctrl Pts',(139.058986731379,0.521711347413453,330.10776011222));
#52725=CARTESIAN_POINT('Ctrl Pts',(139.051574927202,0.391909734077998,330.095664475779));
#52726=CARTESIAN_POINT('Ctrl Pts',(139.044163123025,0.262028659770151,330.088734985367));
#52727=CARTESIAN_POINT('Ctrl Pts',(139.036388044247,0.125781727113219,330.081465859988));
#52728=CARTESIAN_POINT('Ctrl Pts',(139.028612965468,-0.0109832181841689,
330.079859130018));
#52729=CARTESIAN_POINT('Ctrl Pts',(139.02083788669,-0.147756205169704,330.083969979106));
#52730=CARTESIAN_POINT('Ctrl Pts',(139.013072375641,-0.284360884287172,
330.088075769532));
#52731=CARTESIAN_POINT('Ctrl Pts',(139.005306864592,-0.420973198440031,
330.097885128071));
#52732=CARTESIAN_POINT('Ctrl Pts',(138.997541353543,-0.5570791651115,330.113401401148));
#52733=CARTESIAN_POINT('Ctrl Pts',(138.989783542021,-0.693050182321493,
330.128902289796));
#52734=CARTESIAN_POINT('Ctrl Pts',(138.982025730498,-0.828515465290936,
330.150098788414));
#52735=CARTESIAN_POINT('Ctrl Pts',(138.974267918976,-0.96296250200261,330.176942226944));
#52736=CARTESIAN_POINT('Ctrl Pts',(138.966515945453,-1.09730836305528,330.203765464935));
#52737=CARTESIAN_POINT('Ctrl Pts',(138.95876397193,-1.23063712129286,330.236227108192));
#52738=CARTESIAN_POINT('Ctrl Pts',(138.951011998407,-1.36244320542227,330.274226880763));
#52739=CARTESIAN_POINT('Ctrl Pts',(138.943263307849,-1.49419346959636,330.312210560409));
#52740=CARTESIAN_POINT('Ctrl Pts',(138.935514617292,-1.62442196743454,330.355727596477));
#52741=CARTESIAN_POINT('Ctrl Pts',(138.927765926734,-1.75263533029214,330.404627059584));
#52742=CARTESIAN_POINT('Ctrl Pts',(138.920018848356,-1.88082201728869,330.453516348748));
#52743=CARTESIAN_POINT('Ctrl Pts',(138.912271769979,-2.00699403826913,330.50778569827));
#52744=CARTESIAN_POINT('Ctrl Pts',(138.904524691601,-2.13067552867567,330.567235077967));
#52745=CARTESIAN_POINT('Ctrl Pts',(138.896777548295,-2.25435805565244,330.626684955908));
#52746=CARTESIAN_POINT('Ctrl Pts',(138.889030404989,-2.37554965813174,330.691314781282));
#52747=CARTESIAN_POINT('Ctrl Pts',(138.881283261683,-2.49379707634702,330.760877543111));
#52748=CARTESIAN_POINT('Ctrl Pts',(138.873534376655,-2.61207107909245,330.830455944125));
#52749=CARTESIAN_POINT('Ctrl Pts',(138.865785491627,-2.72739924360139,330.904969290283));
#52750=CARTESIAN_POINT('Ctrl Pts',(138.858036606599,-2.83935575491062,330.98412625204));
#52751=CARTESIAN_POINT('Ctrl Pts',(138.850279496824,-2.95143109801757,331.063367231813));
#52752=CARTESIAN_POINT('Ctrl Pts',(138.84252238705,-3.06012731945807,331.147261446876));
#52753=CARTESIAN_POINT('Ctrl Pts',(138.834765277275,-3.16504984818297,331.235475790884));
#52754=CARTESIAN_POINT('Ctrl Pts',(138.827004022349,-3.27002844415259,331.323737273818));
#52755=CARTESIAN_POINT('Ctrl Pts',(138.819242767422,-3.37122904102209,331.41632322196));
#52756=CARTESIAN_POINT('Ctrl Pts',(138.811481512496,-3.4682934040009,331.512863076066));
#52757=CARTESIAN_POINT('Ctrl Pts',(138.803707842092,-3.56551303832708,331.609557362476));
#52758=CARTESIAN_POINT('Ctrl Pts',(138.795934171687,-3.65858295128743,331.710217906844));
#52759=CARTESIAN_POINT('Ctrl Pts',(138.788160501282,-3.74718415282704,331.81443976869));
#52760=CARTESIAN_POINT('Ctrl Pts',(138.780748697105,-3.83166094711786,331.913810077792));
#52761=CARTESIAN_POINT('Ctrl Pts',(138.773336892928,-3.91207552684104,332.016417380716));
#52762=CARTESIAN_POINT('Ctrl Pts',(138.765925088751,-3.98818878504526,332.121887202117));
#52763=CARTESIAN_POINT('Ctrl Pts',(138.758087643193,-4.06867303735473,332.233413891644));
#52764=CARTESIAN_POINT('Ctrl Pts',(138.750250197634,-4.14460103872594,332.348492846247));
#52765=CARTESIAN_POINT('Ctrl Pts',(138.742412752076,-4.21564609093278,332.466719301281));
#52766=CARTESIAN_POINT('Ctrl Pts',(138.734585232324,-4.28660116746858,332.584796027315));
#52767=CARTESIAN_POINT('Ctrl Pts',(138.726757712572,-4.3526854049202,332.706011997598));
#52768=CARTESIAN_POINT('Ctrl Pts',(138.718930192819,-4.41361341164634,332.829930942335));
#52769=CARTESIAN_POINT('Ctrl Pts',(138.711110983938,-4.4744767280467,332.953718316102));
#52770=CARTESIAN_POINT('Ctrl Pts',(138.703291775057,-4.53019454163685,333.080202611903));
#52771=CARTESIAN_POINT('Ctrl Pts',(138.695472566176,-4.58052586943205,333.208920486979));
#52772=CARTESIAN_POINT('Ctrl Pts',(138.687660059247,-4.6308140575474,333.337528036177));
#52773=CARTESIAN_POINT('Ctrl Pts',(138.679847552318,-4.67572481157235,333.468364999081));
#52774=CARTESIAN_POINT('Ctrl Pts',(138.67203504539,-4.71506416979987,333.600945698992));
#52775=CARTESIAN_POINT('Ctrl Pts',(138.66422801327,-4.75437595999206,333.733433489675));
#52776=CARTESIAN_POINT('Ctrl Pts',(138.65642098115,-4.78812402253395,333.867662217685));
#52777=CARTESIAN_POINT('Ctrl Pts',(138.64861394903,-4.8161635297853,334.003128936689));
#52778=CARTESIAN_POINT('Ctrl Pts',(138.640810107855,-4.84419157653209,334.138540286784));
#52779=CARTESIAN_POINT('Ctrl Pts',(138.63300626668,-4.86651563677257,334.275188246238));
#52780=CARTESIAN_POINT('Ctrl Pts',(138.625202425506,-4.88304152665067,334.412557652612));
#52781=CARTESIAN_POINT('Ctrl Pts',(138.617399514567,-4.89956544660317,334.549910684224));
#52782=CARTESIAN_POINT('Ctrl Pts',(138.609596603629,-4.91029252386777,334.687984612255));
#52783=CARTESIAN_POINT('Ctrl Pts',(138.601793692691,-4.915180212012,334.826257242034));
#52784=CARTESIAN_POINT('Ctrl Pts',(138.598468253963,-4.91726324327712,334.88518616762));
#52785=CARTESIAN_POINT('Ctrl Pts',(138.595142815236,-4.91828631742129,334.94415112711));
#52786=CARTESIAN_POINT('Ctrl Pts',(138.591817376508,-4.9182490157254,335.003111561684));
#52787=CARTESIAN_POINT('',(136.841817376545,-4.91824939834121,335.002432738434));
#52788=CARTESIAN_POINT('Ctrl Pts',(138.591817376453,-4.91824901572479,335.003111562653));
#52789=CARTESIAN_POINT('Ctrl Pts',(138.58309093916,-4.91815113059199,335.157832361097));
#52790=CARTESIAN_POINT('Ctrl Pts',(138.574364501866,-4.91074827991025,335.312277323951));
#52791=CARTESIAN_POINT('Ctrl Pts',(138.565638064572,-4.89614264762376,335.465800640424));
#52792=CARTESIAN_POINT('Ctrl Pts',(138.556877973935,-4.88148068898621,335.619916016731));
#52793=CARTESIAN_POINT('Ctrl Pts',(138.548117883297,-4.85956039717657,335.773102436575));
#52794=CARTESIAN_POINT('Ctrl Pts',(138.539357792659,-4.83053502206984,335.924723992906));
#52795=CARTESIAN_POINT('Ctrl Pts',(138.530549670193,-4.80135049999856,336.077176894582));
#52796=CARTESIAN_POINT('Ctrl Pts',(138.521741547726,-4.76498286359781,336.228047539157));
#52797=CARTESIAN_POINT('Ctrl Pts',(138.51293342526,-4.72163668021889,336.376709890468));
#52798=CARTESIAN_POINT('Ctrl Pts',(138.504517968332,-4.68022286693529,336.518744883622));
#52799=CARTESIAN_POINT('Ctrl Pts',(138.496102511405,-4.63243927253342,336.658764102443));
#52800=CARTESIAN_POINT('Ctrl Pts',(138.487687054477,-4.57850424739586,336.796241052609));
#52801=CARTESIAN_POINT('Ctrl Pts',(138.479911975699,-4.52867343333853,336.923256629656));
#52802=CARTESIAN_POINT('Ctrl Pts',(138.472136896921,-4.47347442654302,337.048397755958));
#52803=CARTESIAN_POINT('Ctrl Pts',(138.464361818142,-4.41306828170672,337.171177423311));
#52804=CARTESIAN_POINT('Ctrl Pts',(138.456596307093,-4.35273647047733,337.293806002466));
#52805=CARTESIAN_POINT('Ctrl Pts',(138.448830796044,-4.28721044162563,337.414078557257));
#52806=CARTESIAN_POINT('Ctrl Pts',(138.441065284995,-4.2167000910404,337.531525904414));
#52807=CARTESIAN_POINT('Ctrl Pts',(138.433307473473,-4.14625965167311,337.648856802184));
#52808=CARTESIAN_POINT('Ctrl Pts',(138.425549661951,-4.07084492526617,337.763367733909));
#52809=CARTESIAN_POINT('Ctrl Pts',(138.417791850428,-3.99071254084815,337.874612404972));
#52810=CARTESIAN_POINT('Ctrl Pts',(138.410039876905,-3.91064045859046,337.985773360892));
#52811=CARTESIAN_POINT('Ctrl Pts',(138.402287903382,-3.82585801233367,338.093672632728));
#52812=CARTESIAN_POINT('Ctrl Pts',(138.394535929859,-3.73666592425114,338.197891623092));
#52813=CARTESIAN_POINT('Ctrl Pts',(138.386787239302,-3.64751160907086,338.302066476651));
#52814=CARTESIAN_POINT('Ctrl Pts',(138.379038548744,-3.55395161998393,338.402563852336));
#52815=CARTESIAN_POINT('Ctrl Pts',(138.371289858187,-3.45632772543574,338.498997244481));
#52816=CARTESIAN_POINT('Ctrl Pts',(138.363542779809,-3.35872414235418,338.595410572853));
#52817=CARTESIAN_POINT('Ctrl Pts',(138.355795701431,-3.25705861353494,338.68776132502));
#52818=CARTESIAN_POINT('Ctrl Pts',(138.348048623053,-3.15171034420147,338.775699268845));
#52819=CARTESIAN_POINT('Ctrl Pts',(138.340301479747,-3.04636119194804,338.863637949674));
#52820=CARTESIAN_POINT('Ctrl Pts',(138.332554336442,-2.93732953768893,338.947163497914));
#52821=CARTESIAN_POINT('Ctrl Pts',(138.324807193136,-2.8250279807187,339.025965719012));
#52822=CARTESIAN_POINT('Ctrl Pts',(138.317058308108,-2.71270117597431,339.104785656521));
#52823=CARTESIAN_POINT('Ctrl Pts',(138.30930942308,-2.5971033255634,339.178879929343));
#52824=CARTESIAN_POINT('Ctrl Pts',(138.301560538052,-2.47867599464065,339.247981682646));
#52825=CARTESIAN_POINT('Ctrl Pts',(138.293803428277,-2.36012296372523,339.317156781263));
#52826=CARTESIAN_POINT('Ctrl Pts',(138.286046318502,-2.23873479118307,339.381328577586));
#52827=CARTESIAN_POINT('Ctrl Pts',(138.278289208727,-2.11497812069718,339.440275961184));
#52828=CARTESIAN_POINT('Ctrl Pts',(138.270527953801,-1.99115531860351,339.49925484438));
#52829=CARTESIAN_POINT('Ctrl Pts',(138.262766698875,-1.86496185607697,339.55300359893));
#52830=CARTESIAN_POINT('Ctrl Pts',(138.255005443949,-1.73688341022672,339.601349702183));
#52831=CARTESIAN_POINT('Ctrl Pts',(138.247231773544,-1.60860008060386,339.649773143445));
#52832=CARTESIAN_POINT('Ctrl Pts',(138.23945810314,-1.47842611341864,339.6927765405));
#52833=CARTESIAN_POINT('Ctrl Pts',(138.231684432735,-1.34686221858047,339.730237333016));
#52834=CARTESIAN_POINT('Ctrl Pts',(138.224272628558,-1.22142265469901,339.765954316629));
#52835=CARTESIAN_POINT('Ctrl Pts',(138.216860824381,-1.09471993302537,339.79663303183));
#52836=CARTESIAN_POINT('Ctrl Pts',(138.209449020204,-0.967193940522633,
339.822211001596));
#52837=CARTESIAN_POINT('Ctrl Pts',(138.201673941425,-0.833417519247343,
339.849042623854));
#52838=CARTESIAN_POINT('Ctrl Pts',(138.193898862647,-0.698312326475554,
339.870345645459));
#52839=CARTESIAN_POINT('Ctrl Pts',(138.186123783868,-0.562375053734725,
339.885991952658));
#52840=CARTESIAN_POINT('Ctrl Pts',(138.178358272819,-0.426605060462241,
339.90161900608));
#52841=CARTESIAN_POINT('Ctrl Pts',(138.17059276177,-0.290005409141113,339.911603151117));
#52842=CARTESIAN_POINT('Ctrl Pts',(138.162827250721,-0.153084232702914,
339.915866991711));
#52843=CARTESIAN_POINT('Ctrl Pts',(138.155069439199,-0.0162988140096955,
339.920126604695));
#52844=CARTESIAN_POINT('Ctrl Pts',(138.147311627677,0.120807107216111,339.918677188149));
#52845=CARTESIAN_POINT('Ctrl Pts',(138.139553816155,0.257719355618189,339.911493031273));
#52846=CARTESIAN_POINT('Ctrl Pts',(138.131801842632,0.394528573211468,339.904314280702));
#52847=CARTESIAN_POINT('Ctrl Pts',(138.124049869109,0.531144019313606,339.89140940014));
#52848=CARTESIAN_POINT('Ctrl Pts',(138.116297895586,0.667050948427387,339.872804746212));
#52849=CARTESIAN_POINT('Ctrl Pts',(138.108549205028,0.802900320876047,339.854207971365));
#52850=CARTESIAN_POINT('Ctrl Pts',(138.10080051447,0.938041386672704,339.829916277048));
#52851=CARTESIAN_POINT('Ctrl Pts',(138.093051823913,1.07196417444173,339.800007903245));
#52852=CARTESIAN_POINT('Ctrl Pts',(138.085304745535,1.20585909845621,339.770105752128));
#52853=CARTESIAN_POINT('Ctrl Pts',(138.077557667157,1.33853586738105,339.734589331088));
#52854=CARTESIAN_POINT('Ctrl Pts',(138.069810588779,1.46949475383565,339.69358799118));
#52855=CARTESIAN_POINT('Ctrl Pts',(138.062063445473,1.60045473785176,339.652586307642));
#52856=CARTESIAN_POINT('Ctrl Pts',(138.054316302168,1.72969643766128,339.606099730335));
#52857=CARTESIAN_POINT('Ctrl Pts',(138.046569158862,1.85673572289206,339.554307358736));
#52858=CARTESIAN_POINT('Ctrl Pts',(138.038820273834,1.98380356925116,339.502503343113));
#52859=CARTESIAN_POINT('Ctrl Pts',(138.031071388805,2.10866765385973,339.445391307083));
#52860=CARTESIAN_POINT('Ctrl Pts',(138.023322503777,2.23086461655405,339.383198161743));
#52861=CARTESIAN_POINT('Ctrl Pts',(138.015565394003,2.35319128036728,339.320939003956));
#52862=CARTESIAN_POINT('Ctrl Pts',(138.007808284228,2.47284481835479,339.25358814113));
#52863=CARTESIAN_POINT('Ctrl Pts',(138.000051174453,2.5893867663664,339.181418328351));
#52864=CARTESIAN_POINT('Ctrl Pts',(137.992289919527,2.7059909906687,339.109209950331));
#52865=CARTESIAN_POINT('Ctrl Pts',(137.984528664601,2.81947998860143,339.032177710663));
#52866=CARTESIAN_POINT('Ctrl Pts',(137.976767409675,2.92944585443495,338.950636663683));
#52867=CARTESIAN_POINT('Ctrl Pts',(137.96899373927,3.03958762981602,338.868965177601));
#52868=CARTESIAN_POINT('Ctrl Pts',(137.961220068865,3.14619470686088,338.782770717136));
#52869=CARTESIAN_POINT('Ctrl Pts',(137.953446398461,3.24889305911077,338.692408015504));
#52870=CARTESIAN_POINT('Ctrl Pts',(137.946034594284,3.34681077835521,338.606251719374));
#52871=CARTESIAN_POINT('Ctrl Pts',(137.938622790106,3.4411752773667,338.516306710775));
#52872=CARTESIAN_POINT('Ctrl Pts',(137.931210985929,3.53169596980812,338.422909090137));
#52873=CARTESIAN_POINT('Ctrl Pts',(137.923435907151,3.62665335103383,338.324933773893));
#52874=CARTESIAN_POINT('Ctrl Pts',(137.915660828373,3.71768068852464,338.222849222306));
#52875=CARTESIAN_POINT('Ctrl Pts',(137.907885749594,3.80440146040663,338.117003784174));
#52876=CARTESIAN_POINT('Ctrl Pts',(137.900120238545,3.89101551685791,338.011288595592));
#52877=CARTESIAN_POINT('Ctrl Pts',(137.892354727496,3.97333330683864,337.90182202834));
#52878=CARTESIAN_POINT('Ctrl Pts',(137.884589216447,4.05101476646574,337.788989498793));
#52879=CARTESIAN_POINT('Ctrl Pts',(137.876831404925,4.12861920469948,337.676268843027));
#52880=CARTESIAN_POINT('Ctrl Pts',(137.869073593403,4.20159624051518,337.560189186381));
#52881=CARTESIAN_POINT('Ctrl Pts',(137.86131578188,4.26964600336404,337.441168996292));
#52882=CARTESIAN_POINT('Ctrl Pts',(137.853563808357,4.33764455660831,337.322238372671));
#52883=CARTESIAN_POINT('Ctrl Pts',(137.845811834834,4.40072302410854,337.200371958127));
#52884=CARTESIAN_POINT('Ctrl Pts',(137.838059861311,4.45862501138884,337.076016876212));
#52885=CARTESIAN_POINT('Ctrl Pts',(137.830311170754,4.51650247714317,336.951714458749));
#52886=CARTESIAN_POINT('Ctrl Pts',(137.822562480196,4.56920765824678,336.82492582376));
#52887=CARTESIAN_POINT('Ctrl Pts',(137.814813789639,4.61653037359807,336.6961221572));
#52888=CARTESIAN_POINT('Ctrl Pts',(137.807066711261,4.6638432430632,336.567345289319));
#52889=CARTESIAN_POINT('Ctrl Pts',(137.799319632883,4.70577573955716,336.436554590439));
#52890=CARTESIAN_POINT('Ctrl Pts',(137.791572554505,4.74216620598345,336.304240291253));
#52891=CARTESIAN_POINT('Ctrl Pts',(137.783825411199,4.77855697739688,336.171924883147));
#52892=CARTESIAN_POINT('Ctrl Pts',(137.776078267894,4.80940552244599,336.038086226146));
#52893=CARTESIAN_POINT('Ctrl Pts',(137.768331124588,4.83460045897783,335.903228356813));
#52894=CARTESIAN_POINT('Ctrl Pts',(137.76058223956,4.85980105986628,335.768340168568));
#52895=CARTESIAN_POINT('Ctrl Pts',(137.752833354532,4.87934545121814,335.632432696179));
#52896=CARTESIAN_POINT('Ctrl Pts',(137.745084469504,4.89317369664371,335.496018383706));
#52897=CARTESIAN_POINT('Ctrl Pts',(137.737327359729,4.90701661951185,335.359459279672));
#52898=CARTESIAN_POINT('Ctrl Pts',(137.729570249954,4.9151312372168,335.222392650415));
#52899=CARTESIAN_POINT('Ctrl Pts',(137.721813140179,4.9175096372201,335.085334813221));
#52900=CARTESIAN_POINT('Ctrl Pts',(137.714051885253,4.91988930816432,334.948203736701));
#52901=CARTESIAN_POINT('Ctrl Pts',(137.706290630327,4.9165266631952,334.811081852164));
#52902=CARTESIAN_POINT('Ctrl Pts',(137.698529375401,4.90746589703005,334.67448267022));
#52903=CARTESIAN_POINT('Ctrl Pts',(137.690755704996,4.89839063659193,334.537664974103));
#52904=CARTESIAN_POINT('Ctrl Pts',(137.682982034592,4.8835990824101,334.401372040259));
#52905=CARTESIAN_POINT('Ctrl Pts',(137.675208364187,4.86318713003702,334.266110362015));
#52906=CARTESIAN_POINT('Ctrl Pts',(137.66779656001,4.84372535895781,334.137145147436));
#52907=CARTESIAN_POINT('Ctrl Pts',(137.660384755833,4.81915472738283,334.009117621842));
#52908=CARTESIAN_POINT('Ctrl Pts',(137.652972951656,4.78960061639348,333.882454028711));
#52909=CARTESIAN_POINT('Ctrl Pts',(137.645197872877,4.7585979703873,333.74958227557));
#52910=CARTESIAN_POINT('Ctrl Pts',(137.637422794099,4.722013008543,333.617791637017));
#52911=CARTESIAN_POINT('Ctrl Pts',(137.62964771532,4.67993490720645,333.487587249852));
#52912=CARTESIAN_POINT('Ctrl Pts',(137.621882204271,4.6379085856524,333.357543087474));
#52913=CARTESIAN_POINT('Ctrl Pts',(137.614116693222,4.59040269343587,333.229081660976));
#52914=CARTESIAN_POINT('Ctrl Pts',(137.606351182173,4.5375573073284,333.102697508247));
#52915=CARTESIAN_POINT('Ctrl Pts',(137.598593370651,4.48476431757512,332.976438665774));
#52916=CARTESIAN_POINT('Ctrl Pts',(137.590835559129,4.42664251935187,332.852253356599));
#52917=CARTESIAN_POINT('Ctrl Pts',(137.583077747607,4.36338153369391,332.730620205008));
#52918=CARTESIAN_POINT('Ctrl Pts',(137.575325774084,4.30016815393381,332.60907858622));
#52919=CARTESIAN_POINT('Ctrl Pts',(137.567573800561,4.23182346424373,332.490085647576));
#52920=CARTESIAN_POINT('Ctrl Pts',(137.559821827038,4.15858471059526,332.37409896087));
#52921=CARTESIAN_POINT('Ctrl Pts',(137.55207313648,4.08537697360243,332.258161394595));
#52922=CARTESIAN_POINT('Ctrl Pts',(137.544324445923,4.00727950324135,332.145227877867));
#52923=CARTESIAN_POINT('Ctrl Pts',(137.536575755365,3.92457478877911,332.035730142214));
#52924=CARTESIAN_POINT('Ctrl Pts',(137.528828676987,3.84188728172347,331.926255188479));
#52925=CARTESIAN_POINT('Ctrl Pts',(137.521081598609,3.75459467267662,331.820214905654));
#52926=CARTESIAN_POINT('Ctrl Pts',(137.513334520231,3.66302172515755,331.718010526598));
#52927=CARTESIAN_POINT('Ctrl Pts',(137.505587376926,3.57144801016907,331.61580529097));
#52928=CARTESIAN_POINT('Ctrl Pts',(137.49784023362,3.47559414598997,331.51743631435));
#52929=CARTESIAN_POINT('Ctrl Pts',(137.490093090314,3.37582371244424,331.423270023471));
#52930=CARTESIAN_POINT('Ctrl Pts',(137.482344205286,3.27603084838684,331.329082562011));
#52931=CARTESIAN_POINT('Ctrl Pts',(137.474595320258,3.17231994701299,331.239099934683));
#52932=CARTESIAN_POINT('Ctrl Pts',(137.46684643523,3.06508949844719,331.153649856161));
#52933=CARTESIAN_POINT('Ctrl Pts',(137.459089325455,2.95774523437535,331.068109080043));
#52934=CARTESIAN_POINT('Ctrl Pts',(137.45133221568,2.84687426690146,330.987110706925));
#52935=CARTESIAN_POINT('Ctrl Pts',(137.443575105906,2.73290649631855,330.910940799538));
#52936=CARTESIAN_POINT('Ctrl Pts',(137.435813850979,2.61887782500306,330.834730189389));
#52937=CARTESIAN_POINT('Ctrl Pts',(137.428052596053,2.50174938678771,330.763353389507));
#52938=CARTESIAN_POINT('Ctrl Pts',(137.420291341127,2.38197691999697,330.69705112567));
#52939=CARTESIAN_POINT('Ctrl Pts',(137.412517670722,2.26201285629313,330.630642799817));
#52940=CARTESIAN_POINT('Ctrl Pts',(137.404744000318,2.13939666183432,330.569325406303));
#52941=CARTESIAN_POINT('Ctrl Pts',(137.396970329913,2.01460615225117,330.513292397112));
#52942=CARTESIAN_POINT('Ctrl Pts',(137.389558525736,1.89562467091261,330.45986773798));
#52943=CARTESIAN_POINT('Ctrl Pts',(137.382146721559,1.77466701468582,330.411246665947));
#52944=CARTESIAN_POINT('Ctrl Pts',(137.374734917382,1.65215947170289,330.367554410189));
#52945=CARTESIAN_POINT('Ctrl Pts',(137.366959838603,1.52364746910659,330.321720666823));
#52946=CARTESIAN_POINT('Ctrl Pts',(137.359184759825,1.39302368741873,330.281166265078));
#52947=CARTESIAN_POINT('Ctrl Pts',(137.351409681047,1.2607611653886,330.246089573167));
#52948=CARTESIAN_POINT('Ctrl Pts',(137.343644169998,1.12866140081207,330.211056045359));
#52949=CARTESIAN_POINT('Ctrl Pts',(137.335878658949,0.994927282499733,330.181486914625));
#52950=CARTESIAN_POINT('Ctrl Pts',(137.3281131479,0.860050481492069,330.157532010247));
#52951=CARTESIAN_POINT('Ctrl Pts',(137.320355336377,0.725307411225288,330.133600857226));
#52952=CARTESIAN_POINT('Ctrl Pts',(137.312597524855,0.589424295316403,330.11527292078));
#52953=CARTESIAN_POINT('Ctrl Pts',(137.304839713333,0.452906233959485,330.102647755599));
#52954=CARTESIAN_POINT('Ctrl Pts',(137.29708773981,0.316490906772975,330.090032091255));
#52955=CARTESIAN_POINT('Ctrl Pts',(137.289335766287,0.179441972855275,330.083110691971));
#52956=CARTESIAN_POINT('Ctrl Pts',(137.281583792764,0.0422726014990651,
330.081931670903));
#52957=CARTESIAN_POINT('Ctrl Pts',(137.273835102206,-0.0948386785468911,
330.080753149152));
#52958=CARTESIAN_POINT('Ctrl Pts',(137.266086411649,-0.232069904538951,
330.085312172089));
#52959=CARTESIAN_POINT('Ctrl Pts',(137.258337721091,-0.368905153072199,
330.095604823168));
#52960=CARTESIAN_POINT('Ctrl Pts',(137.250590642713,-0.505711931889073,
330.105895332774));
#52961=CARTESIAN_POINT('Ctrl Pts',(137.242843564335,-0.642122507591071,
330.121917068401));
#52962=CARTESIAN_POINT('Ctrl Pts',(137.235096485958,-0.777623726731592,
330.143614059599));
#52963=CARTESIAN_POINT('Ctrl Pts',(137.227349342652,-0.913126081502839,
330.165311232639));
#52964=CARTESIAN_POINT('Ctrl Pts',(137.219602199346,-1.04771867855369,330.19268369432));
#52965=CARTESIAN_POINT('Ctrl Pts',(137.21185505604,-1.18089662792125,330.225623997142));
#52966=CARTESIAN_POINT('Ctrl Pts',(137.204106171012,-1.31410451851905,330.258571705644));
#52967=CARTESIAN_POINT('Ctrl Pts',(137.196357285984,-1.44589674919798,330.297089652335));
#52968=CARTESIAN_POINT('Ctrl Pts',(137.188608400956,-1.57578209182491,330.341020083582));
#52969=CARTESIAN_POINT('Ctrl Pts',(137.180851291181,-1.70580529609669,330.384997143044));
#52970=CARTESIAN_POINT('Ctrl Pts',(137.173094181406,-1.83391719835138,330.434398037541));
#52971=CARTESIAN_POINT('Ctrl Pts',(137.165337071632,-1.95964459861807,330.489016059704));
#52972=CARTESIAN_POINT('Ctrl Pts',(137.157575816706,-2.08543918358747,330.543663267992));
#52973=CARTESIAN_POINT('Ctrl Pts',(137.149814561779,-2.20884637611177,330.603532988498));
#52974=CARTESIAN_POINT('Ctrl Pts',(137.142053306853,-2.32941711859297,330.66837225167));
#52975=CARTESIAN_POINT('Ctrl Pts',(137.134279636448,-2.45018073496818,330.733315236532));
#52976=CARTESIAN_POINT('Ctrl Pts',(137.126505966044,-2.56809849786118,330.803243450332));
#52977=CARTESIAN_POINT('Ctrl Pts',(137.118732295639,-2.68274915591487,330.877859775682));
#52978=CARTESIAN_POINT('Ctrl Pts',(137.111320491462,-2.79206279825319,330.949002693136));
#52979=CARTESIAN_POINT('Ctrl Pts',(137.103908687285,-2.89840642334555,331.024406914823));
#52980=CARTESIAN_POINT('Ctrl Pts',(137.096496883108,-3.00144403433597,331.10378173465));
#52981=CARTESIAN_POINT('Ctrl Pts',(137.0888096411,-3.10831073408376,331.186106285428));
#52982=CARTESIAN_POINT('Ctrl Pts',(137.081122399092,-3.21197535388208,331.272975499635));
#52983=CARTESIAN_POINT('Ctrl Pts',(137.073435157085,-3.31202019753984,331.364108737381));
#52984=CARTESIAN_POINT('Ctrl Pts',(137.065757414217,-3.41194141559018,331.455129361608));
#52985=CARTESIAN_POINT('Ctrl Pts',(137.058079671349,-3.50825146044264,331.550403263087));
#52986=CARTESIAN_POINT('Ctrl Pts',(137.050401928481,-3.60056292736444,331.64960753514));
#52987=CARTESIAN_POINT('Ctrl Pts',(137.042731734852,-3.69278362784953,331.748714263318));
#52988=CARTESIAN_POINT('Ctrl Pts',(137.035061541224,-3.78101330033598,331.851743383204));
#52989=CARTESIAN_POINT('Ctrl Pts',(137.027391347595,-3.86489924062372,331.958333199983));
#52990=CARTESIAN_POINT('Ctrl Pts',(137.019659098802,-3.94946385424595,332.065785374222));
#52991=CARTESIAN_POINT('Ctrl Pts',(137.011926850008,-4.02961382326933,332.17685584937));
#52992=CARTESIAN_POINT('Ctrl Pts',(137.004194601214,-4.10502693804777,332.291137341909));
#52993=CARTESIAN_POINT('Ctrl Pts',(136.996533077252,-4.17975026903995,332.404373531904));
#52994=CARTESIAN_POINT('Ctrl Pts',(136.98887155329,-4.2498228205061,332.520761897589));
#52995=CARTESIAN_POINT('Ctrl Pts',(136.981210029328,-4.31497315532209,332.639875060225));
#52996=CARTESIAN_POINT('Ctrl Pts',(136.97354976724,-4.3801127597011,332.758968604599));
#52997=CARTESIAN_POINT('Ctrl Pts',(136.965889505151,-4.44033156764303,332.880785702081));
#52998=CARTESIAN_POINT('Ctrl Pts',(136.958229243063,-4.49540342799684,333.004873166424));
#52999=CARTESIAN_POINT('Ctrl Pts',(136.950568494165,-4.55047878816579,333.128968516522));
#53000=CARTESIAN_POINT('Ctrl Pts',(136.942907745268,-4.60040638841005,333.25533415402));
#53001=CARTESIAN_POINT('Ctrl Pts',(136.93524699637,-4.64500789524381,333.38349614426));
#53002=CARTESIAN_POINT('Ctrl Pts',(136.927461194718,-4.69033746944431,333.513750228902));
#53003=CARTESIAN_POINT('Ctrl Pts',(136.919675393066,-4.73016538867476,333.645859426881));
#53004=CARTESIAN_POINT('Ctrl Pts',(136.911889591414,-4.76435723487632,333.779310358452));
#53005=CARTESIAN_POINT('Ctrl Pts',(136.904218941153,-4.7980433863726,333.910787561284));
#53006=CARTESIAN_POINT('Ctrl Pts',(136.896548290893,-4.82625901319341,334.043566673714));
#53007=CARTESIAN_POINT('Ctrl Pts',(136.888877640632,-4.84892739854841,334.177147555083));
#53008=CARTESIAN_POINT('Ctrl Pts',(136.881034263284,-4.87210622878695,334.313736400026));
#53009=CARTESIAN_POINT('Ctrl Pts',(136.873190885936,-4.88948496247125,334.451163108186));
#53010=CARTESIAN_POINT('Ctrl Pts',(136.865347508588,-4.90103778268651,334.588889655714));
#53011=CARTESIAN_POINT('Ctrl Pts',(136.857504131241,-4.91259060290177,334.726616203242));
#53012=CARTESIAN_POINT('Ctrl Pts',(136.849660753893,-4.91831755439441,334.864642146975));
#53013=CARTESIAN_POINT('Ctrl Pts',(136.841817376545,-4.91824939834121,335.002432738434));
#53014=CARTESIAN_POINT('',(135.091817376461,-4.91824801995541,334.995586758035));
#53015=CARTESIAN_POINT('Ctrl Pts',(136.841817376508,-4.91824939834089,335.00243273908));
#53016=CARTESIAN_POINT('Ctrl Pts',(136.83396453395,-4.91818116002039,335.140389613106));
#53017=CARTESIAN_POINT('Ctrl Pts',(136.826111691392,-4.91230893124131,335.27819838096));
#53018=CARTESIAN_POINT('Ctrl Pts',(136.818258848834,-4.90066665130595,335.415511053136));
#53019=CARTESIAN_POINT('Ctrl Pts',(136.810483770055,-4.8891396605396,335.551463968978));
#53020=CARTESIAN_POINT('Ctrl Pts',(136.802708691277,-4.8719328169481,335.68715168536));
#53021=CARTESIAN_POINT('Ctrl Pts',(136.794933612498,-4.84906155608663,335.822061486619));
#53022=CARTESIAN_POINT('Ctrl Pts',(136.787168101449,-4.82621843976769,335.956805272779));
#53023=CARTESIAN_POINT('Ctrl Pts',(136.7794025904,-4.79772484003616,336.090772666826));
#53024=CARTESIAN_POINT('Ctrl Pts',(136.771637079351,-4.76364808905692,336.223454104625));
#53025=CARTESIAN_POINT('Ctrl Pts',(136.763879267829,-4.72960512527555,336.356003988393));
#53026=CARTESIAN_POINT('Ctrl Pts',(136.756121456307,-4.68999012323058,336.487270077145));
#53027=CARTESIAN_POINT('Ctrl Pts',(136.748363644785,-4.64492173574745,336.616751412952));
#53028=CARTESIAN_POINT('Ctrl Pts',(136.740611671262,-4.59988726365504,336.746135309947));
#53029=CARTESIAN_POINT('Ctrl Pts',(136.732859697739,-4.54940770260102,336.873736759671));
#53030=CARTESIAN_POINT('Ctrl Pts',(136.725107724216,-4.49365186749657,336.999068772265));
#53031=CARTESIAN_POINT('Ctrl Pts',(136.717359033658,-4.43791964502142,337.124347706677));
#53032=CARTESIAN_POINT('Ctrl Pts',(136.7096103431,-4.37691575131309,337.247358759147));
#53033=CARTESIAN_POINT('Ctrl Pts',(136.701861652543,-4.31085749670005,337.367633988953));
#53034=CARTESIAN_POINT('Ctrl Pts',(136.694114574165,-4.24481298605862,337.487884194493));
#53035=CARTESIAN_POINT('Ctrl Pts',(136.686367495787,-4.17371639427106,337.605399367181));
#53036=CARTESIAN_POINT('Ctrl Pts',(136.678620417409,-4.09783126049797,337.719735653145));
#53037=CARTESIAN_POINT('Ctrl Pts',(136.670873274103,-4.02194549073439,337.834072897356));
#53038=CARTESIAN_POINT('Ctrl Pts',(136.663126130798,-3.9412713150868,337.94523087603));
#53039=CARTESIAN_POINT('Ctrl Pts',(136.655378987492,-3.85611570058006,338.05279458304));
#53040=CARTESIAN_POINT('Ctrl Pts',(136.647630102464,-3.77094094128306,338.160382472656));
#53041=CARTESIAN_POINT('Ctrl Pts',(136.639881217436,-3.68128298084066,338.264374176238));
#53042=CARTESIAN_POINT('Ctrl Pts',(136.632132332408,-3.5874889119204,338.36438796356));
#53043=CARTESIAN_POINT('Ctrl Pts',(136.624375222633,-3.49359528900647,338.464507906549));
#53044=CARTESIAN_POINT('Ctrl Pts',(136.616618112858,-3.39555705576614,338.56064121347));
#53045=CARTESIAN_POINT('Ctrl Pts',(136.608861003083,-3.29375839067746,338.652442843679));
#53046=CARTESIAN_POINT('Ctrl Pts',(136.601099748157,-3.19190532763704,338.744293529744));
#53047=CARTESIAN_POINT('Ctrl Pts',(136.593338493231,-3.08628812955419,338.831807677567));
#53048=CARTESIAN_POINT('Ctrl Pts',(136.585577238305,-2.97732307791898,338.914681385782));
#53049=CARTESIAN_POINT('Ctrl Pts',(136.5778035679,-2.86818371771286,338.997687664922));
#53050=CARTESIAN_POINT('Ctrl Pts',(136.570029897496,-2.7556861230471,339.076038447212));
#53051=CARTESIAN_POINT('Ctrl Pts',(136.562256227091,-2.64027523614145,339.149473429234));
#53052=CARTESIAN_POINT('Ctrl Pts',(136.554844422914,-2.5302367537881,339.219489995175));
#53053=CARTESIAN_POINT('Ctrl Pts',(136.547432618737,-2.41755035166708,339.285037977773));
#53054=CARTESIAN_POINT('Ctrl Pts',(136.54002081456,-2.30261981609416,339.345932011092));
#53055=CARTESIAN_POINT('Ctrl Pts',(136.532245735781,-2.18205619261169,339.409810642378));
#53056=CARTESIAN_POINT('Ctrl Pts',(136.524470657003,-2.05864188673958,339.468769449604));
#53057=CARTESIAN_POINT('Ctrl Pts',(136.516695578225,-1.93281640508159,339.522543952992));
#53058=CARTESIAN_POINT('Ctrl Pts',(136.508930067176,-1.80714575968917,339.576252283431));
#53059=CARTESIAN_POINT('Ctrl Pts',(136.501164556127,-1.67907019818954,339.624788851499));
#53060=CARTESIAN_POINT('Ctrl Pts',(136.493399045078,-1.54905466123114,339.667934523857));
#53061=CARTESIAN_POINT('Ctrl Pts',(136.485641233555,-1.41916803505622,339.711037417156));
#53062=CARTESIAN_POINT('Ctrl Pts',(136.477883422033,-1.2873456298699,339.748759929458));
#53063=CARTESIAN_POINT('Ctrl Pts',(136.470125610511,-1.15407292173654,339.780930741374));
#53064=CARTESIAN_POINT('Ctrl Pts',(136.462373636988,-1.02090050554241,339.813077343734));
#53065=CARTESIAN_POINT('Ctrl Pts',(136.454621663465,-0.886280337208536,
339.839680470125));
#53066=CARTESIAN_POINT('Ctrl Pts',(136.446869689942,-0.750713292333256,
339.860618542451));
#53067=CARTESIAN_POINT('Ctrl Pts',(136.439120999384,-0.615203660182013,
339.88154774749));
#53068=CARTESIAN_POINT('Ctrl Pts',(136.431372308827,-0.478748334545758,
339.896816610674));
#53069=CARTESIAN_POINT('Ctrl Pts',(136.423623618269,-0.341858415849529,
339.906354643318));
#53070=CARTESIAN_POINT('Ctrl Pts',(136.415876539891,-0.204996978244212,
339.915890691495));
#53071=CARTESIAN_POINT('Ctrl Pts',(136.408129461513,-0.0677015171162233,
339.919698253643));
#53072=CARTESIAN_POINT('Ctrl Pts',(136.400382383136,0.0695121051806816,
339.917758750664));
#53073=CARTESIAN_POINT('Ctrl Pts',(136.39263523983,0.206726877459855,339.915819231431));
#53074=CARTESIAN_POINT('Ctrl Pts',(136.384888096524,0.34385941870464,339.908132556525));
#53075=CARTESIAN_POINT('Ctrl Pts',(136.377140953218,0.480394623938193,339.894732277438));
#53076=CARTESIAN_POINT('Ctrl Pts',(136.36939206819,0.616960525184561,339.881328985684));
#53077=CARTESIAN_POINT('Ctrl Pts',(136.361643183162,0.75292843426079,339.862209571831));
#53078=CARTESIAN_POINT('Ctrl Pts',(136.353894298134,0.887789514315184,339.837459337377));
#53079=CARTESIAN_POINT('Ctrl Pts',(136.346137188359,1.02279373731342,339.812682832768));
#53080=CARTESIAN_POINT('Ctrl Pts',(136.338380078584,1.15668839945633,339.782263639385));
#53081=CARTESIAN_POINT('Ctrl Pts',(136.33062296881,1.28897544768678,339.746338099816));
#53082=CARTESIAN_POINT('Ctrl Pts',(136.322861713884,1.42133318588603,339.710393362786));
#53083=CARTESIAN_POINT('Ctrl Pts',(136.315100458957,1.55208122601918,339.668936534622));
#53084=CARTESIAN_POINT('Ctrl Pts',(136.307339204031,1.68073873714333,339.622153216842));
#53085=CARTESIAN_POINT('Ctrl Pts',(136.299565533627,1.8096020583559,339.575295061001));
#53086=CARTESIAN_POINT('Ctrl Pts',(136.291791863222,1.93636780630809,339.523093537679));
#53087=CARTESIAN_POINT('Ctrl Pts',(136.284018192817,2.06057630253733,339.465781943168));
#53088=CARTESIAN_POINT('Ctrl Pts',(136.27660638864,2.17900286338367,339.411138217169));
#53089=CARTESIAN_POINT('Ctrl Pts',(136.269194584463,2.29510463848692,339.351849592093));
#53090=CARTESIAN_POINT('Ctrl Pts',(136.261782780286,2.40850723773322,339.288155308322));
#53091=CARTESIAN_POINT('Ctrl Pts',(136.254007701508,2.52746803617814,339.221339177967));
#53092=CARTESIAN_POINT('Ctrl Pts',(136.246232622729,2.6438343174242,339.149463448876));
#53093=CARTESIAN_POINT('Ctrl Pts',(136.238457543951,2.75714583254226,339.072754586345));
#53094=CARTESIAN_POINT('Ctrl Pts',(136.230692032902,2.87031791062721,338.996140118953));
#53095=CARTESIAN_POINT('Ctrl Pts',(136.222926521853,2.98044238149894,338.914704568925));
#53096=CARTESIAN_POINT('Ctrl Pts',(136.215161010804,3.08708336519596,338.828720329148));
#53097=CARTESIAN_POINT('Ctrl Pts',(136.207403199282,3.19361861404717,338.742821342995));
#53098=CARTESIAN_POINT('Ctrl Pts',(136.199645387759,3.29667694683085,338.65238288609));
#53099=CARTESIAN_POINT('Ctrl Pts',(136.191887576237,3.39585157846239,338.557720494861));
#53100=CARTESIAN_POINT('Ctrl Pts',(136.184135602714,3.49495157803855,338.463129340083));
#53101=CARTESIAN_POINT('Ctrl Pts',(136.176383629191,3.59017341216274,338.364320846713));
#53102=CARTESIAN_POINT('Ctrl Pts',(136.168631655668,3.68114379069314,338.261650418843));
#53103=CARTESIAN_POINT('Ctrl Pts',(136.160882965111,3.77207564321429,338.159023471961));
#53104=CARTESIAN_POINT('Ctrl Pts',(136.153134274553,3.8587593625195,338.052538135483));
#53105=CARTESIAN_POINT('Ctrl Pts',(136.145385583995,3.94085908740338,337.942586059188));
#53106=CARTESIAN_POINT('Ctrl Pts',(136.137638505617,4.02294173075376,337.832656859342));
#53107=CARTESIAN_POINT('Ctrl Pts',(136.12989142724,4.10044204302277,337.719262667365));
#53108=CARTESIAN_POINT('Ctrl Pts',(136.122144348862,4.17306523793142,337.602827228701));
#53109=CARTESIAN_POINT('Ctrl Pts',(136.114397205556,4.24568904149237,337.486390814196));
#53110=CARTESIAN_POINT('Ctrl Pts',(136.10665006225,4.31343543930706,337.366913433816));
#53111=CARTESIAN_POINT('Ctrl Pts',(136.098902918944,4.37605389268097,337.244846406962));
#53112=CARTESIAN_POINT('Ctrl Pts',(136.091154033916,4.43868642401258,337.12275193685));
#53113=CARTESIAN_POINT('Ctrl Pts',(136.083405148888,4.49618853844671,336.998067009452));
#53114=CARTESIAN_POINT('Ctrl Pts',(136.07565626386,4.54835660701591,336.871265678068));
#53115=CARTESIAN_POINT('Ctrl Pts',(136.067899154085,4.60058004731211,336.744329758441));
#53116=CARTESIAN_POINT('Ctrl Pts',(136.060142044311,4.64745798319112,336.615273309535));
#53117=CARTESIAN_POINT('Ctrl Pts',(136.052384934536,4.68883554295597,336.484588937589));
#53118=CARTESIAN_POINT('Ctrl Pts',(136.04462367961,4.73023521356575,336.353834732094));
#53119=CARTESIAN_POINT('Ctrl Pts',(136.036862424684,4.76612854915706,336.221451247247));
#53120=CARTESIAN_POINT('Ctrl Pts',(136.029101169757,4.7964114207934,336.087943263678));
#53121=CARTESIAN_POINT('Ctrl Pts',(136.021327499353,4.8267427351552,335.954221710846));
#53122=CARTESIAN_POINT('Ctrl Pts',(136.013553828948,4.85144558055753,335.819372449372));
#53123=CARTESIAN_POINT('Ctrl Pts',(136.005780158543,4.87046738243523,335.683908282692));
#53124=CARTESIAN_POINT('Ctrl Pts',(135.998368354366,4.88860371485924,335.554750005561));
#53125=CARTESIAN_POINT('Ctrl Pts',(135.990956550189,4.90157597759195,335.425033068943));
#53126=CARTESIAN_POINT('Ctrl Pts',(135.983544746012,4.90938274900289,335.295201772171));
#53127=CARTESIAN_POINT('Ctrl Pts',(135.975769667233,4.9175721535358,335.159007056798));
#53128=CARTESIAN_POINT('Ctrl Pts',(135.967994588455,4.92010279141976,335.022256087093));
#53129=CARTESIAN_POINT('Ctrl Pts',(135.960219509677,4.91691603504921,334.885458449565));
#53130=CARTESIAN_POINT('Ctrl Pts',(135.952453998628,4.91373320018525,334.74882915024));
#53131=CARTESIAN_POINT('Ctrl Pts',(135.944688487579,4.90484697894459,334.61215368439));
#53132=CARTESIAN_POINT('Ctrl Pts',(135.93692297653,4.89025055265981,334.475946000196));
#53133=CARTESIAN_POINT('Ctrl Pts',(135.929165165007,4.87566859877419,334.339873366317));
#53134=CARTESIAN_POINT('Ctrl Pts',(135.921407353485,4.85538774829809,334.204267977238));
#53135=CARTESIAN_POINT('Ctrl Pts',(135.913649541963,4.82945320779463,334.06964266208));
#53136=CARTESIAN_POINT('Ctrl Pts',(135.90589756844,4.80353818385534,333.935118656741));
#53137=CARTESIAN_POINT('Ctrl Pts',(135.898145594917,4.77197801206601,333.801573639564));
#53138=CARTESIAN_POINT('Ctrl Pts',(135.890393621394,4.73486955059473,333.669513847742));
#53139=CARTESIAN_POINT('Ctrl Pts',(135.882644930836,4.69777680457891,333.53750998332));
#53140=CARTESIAN_POINT('Ctrl Pts',(135.874896240279,4.65514054779613,333.406990468744));
#53141=CARTESIAN_POINT('Ctrl Pts',(135.867147549721,4.60710837313153,333.278449681037));
#53142=CARTESIAN_POINT('Ctrl Pts',(135.859400471343,4.55908619196203,333.149935637314));
#53143=CARTESIAN_POINT('Ctrl Pts',(135.851653392965,4.50567046270539,333.023399867495));
#53144=CARTESIAN_POINT('Ctrl Pts',(135.843906314588,4.44705799617459,332.899319576623));
#53145=CARTESIAN_POINT('Ctrl Pts',(135.836159171282,4.3884450384149,332.775238245839));
#53146=CARTESIAN_POINT('Ctrl Pts',(135.828412027976,4.32463542346004,332.653612788476));
#53147=CARTESIAN_POINT('Ctrl Pts',(135.82066488467,4.25587309455981,332.534898122693));
#53148=CARTESIAN_POINT('Ctrl Pts',(135.812915999642,4.18709530642819,332.416156767333));
#53149=CARTESIAN_POINT('Ctrl Pts',(135.805167114614,4.11336278453372,332.300327843917));
#53150=CARTESIAN_POINT('Ctrl Pts',(135.797418229586,4.03496397509108,332.187839125829));
#53151=CARTESIAN_POINT('Ctrl Pts',(135.789661119811,3.95648195234205,332.075231011054));
#53152=CARTESIAN_POINT('Ctrl Pts',(135.781904010036,3.87332397211809,331.965970504916));
#53153=CARTESIAN_POINT('Ctrl Pts',(135.774146900262,3.78582046755282,331.860454419831));
#53154=CARTESIAN_POINT('Ctrl Pts',(135.766385645335,3.69827020391256,331.754881950324));
#53155=CARTESIAN_POINT('Ctrl Pts',(135.758624390409,3.60637005067453,331.653058178861));
#53156=CARTESIAN_POINT('Ctrl Pts',(135.750863135483,3.51048813849675,331.55534383545));
#53157=CARTESIAN_POINT('Ctrl Pts',(135.743089465078,3.41445284650732,331.457473180934));
#53158=CARTESIAN_POINT('Ctrl Pts',(135.735315794674,3.31442335274736,331.363725358191));
#53159=CARTESIAN_POINT('Ctrl Pts',(135.727542124269,3.21080243345159,331.274422085657));
#53160=CARTESIAN_POINT('Ctrl Pts',(135.720130320092,3.11200509287935,331.189275901945));
#53161=CARTESIAN_POINT('Ctrl Pts',(135.712718515915,3.00994338920189,331.108169971903));
#53162=CARTESIAN_POINT('Ctrl Pts',(135.705306711738,2.90499017388142,331.031345926872));
#53163=CARTESIAN_POINT('Ctrl Pts',(135.69753163296,2.79489288883805,330.950756506548));
#53164=CARTESIAN_POINT('Ctrl Pts',(135.689756554181,2.68126555432611,330.874624642686));
#53165=CARTESIAN_POINT('Ctrl Pts',(135.681981475403,2.56450496575192,330.803275402992));
#53166=CARTESIAN_POINT('Ctrl Pts',(135.674215964354,2.4478880585154,330.732013963079));
#53167=CARTESIAN_POINT('Ctrl Pts',(135.666450453305,2.32814589923475,330.665523639092));
#53168=CARTESIAN_POINT('Ctrl Pts',(135.658684942256,2.20570698792708,330.604088291843));
#53169=CARTESIAN_POINT('Ctrl Pts',(135.650927130733,2.08338947515639,330.54271385792));
#53170=CARTESIAN_POINT('Ctrl Pts',(135.643169319211,1.95838087855779,330.486384600692));
#53171=CARTESIAN_POINT('Ctrl Pts',(135.635411507689,1.8311369109464,330.435340026259));
#53172=CARTESIAN_POINT('Ctrl Pts',(135.627659534166,1.70398869845582,330.384333864488));
#53173=CARTESIAN_POINT('Ctrl Pts',(135.619907560643,1.57460882457687,330.338604614647));
#53174=CARTESIAN_POINT('Ctrl Pts',(135.61215558712,1.44347541047631,330.298344780628));
#53175=CARTESIAN_POINT('Ctrl Pts',(135.604406896562,1.31239753145448,330.258101996673));
#53176=CARTESIAN_POINT('Ctrl Pts',(135.596658206005,1.17956796212342,330.223324136061));
#53177=CARTESIAN_POINT('Ctrl Pts',(135.588909515447,1.04548230564657,330.19415462056));
#53178=CARTESIAN_POINT('Ctrl Pts',(135.581162437069,0.911424546810491,330.164991174022));
#53179=CARTESIAN_POINT('Ctrl Pts',(135.573415358692,0.776111602352436,330.141433834658));
#53180=CARTESIAN_POINT('Ctrl Pts',(135.565668280314,0.640051269799193,330.123575343089));
#53181=CARTESIAN_POINT('Ctrl Pts',(135.557921137008,0.503989796929267,330.105716701849));
#53182=CARTESIAN_POINT('Ctrl Pts',(135.550173993702,0.367181311020722,330.093557054537));
#53183=CARTESIAN_POINT('Ctrl Pts',(135.542426850396,0.230140374147949,330.087137446388));
#53184=CARTESIAN_POINT('Ctrl Pts',(135.534677965368,0.0930686275632914,
330.080716394974));
#53185=CARTESIAN_POINT('Ctrl Pts',(135.52692908034,-0.0442352836071517,
330.080037968927));
#53186=CARTESIAN_POINT('Ctrl Pts',(135.519180195312,-0.181255540800347,
330.085091100394));
#53187=CARTESIAN_POINT('Ctrl Pts',(135.511423085537,-0.318421232710352,
330.090149595307));
#53188=CARTESIAN_POINT('Ctrl Pts',(135.503665975763,-0.45530227799531,330.100951785737));
#53189=CARTESIAN_POINT('Ctrl Pts',(135.495908865988,-0.591386172300536,
330.11743454138));
#53190=CARTESIAN_POINT('Ctrl Pts',(135.488147611062,-0.72754278548776,330.13392610488));
#53191=CARTESIAN_POINT('Ctrl Pts',(135.480386356136,-0.862901013372442,
330.156104218956));
#53192=CARTESIAN_POINT('Ctrl Pts',(135.47262510121,-0.996958293773339,330.18385452639));
#53193=CARTESIAN_POINT('Ctrl Pts',(135.464851430805,-1.13123002213371,330.211649225271));
#53194=CARTESIAN_POINT('Ctrl Pts',(135.4570777604,-1.26419626506519,330.245033834474));
#53195=CARTESIAN_POINT('Ctrl Pts',(135.449304089996,-1.39536851733881,330.283843751176));
#53196=CARTESIAN_POINT('Ctrl Pts',(135.441892285818,-1.5204346697122,330.320847056919));
#53197=CARTESIAN_POINT('Ctrl Pts',(135.434480481641,-1.64386982076507,330.36278184833));
#53198=CARTESIAN_POINT('Ctrl Pts',(135.427068677464,-1.76526900622609,330.409465347244));
#53199=CARTESIAN_POINT('Ctrl Pts',(135.419293598686,-1.89261832739498,330.458436943502));
#53200=CARTESIAN_POINT('Ctrl Pts',(135.411518519907,-2.01812950655818,330.512789273245));
#53201=CARTESIAN_POINT('Ctrl Pts',(135.403743441129,-2.1413144585852,330.572364575538));
#53202=CARTESIAN_POINT('Ctrl Pts',(135.39597793008,-2.26434782368662,330.631866566629));
#53203=CARTESIAN_POINT('Ctrl Pts',(135.388212419031,-2.38506030882731,330.696578573431));
#53204=CARTESIAN_POINT('Ctrl Pts',(135.380446907982,-2.50298132344674,330.766293874514));
#53205=CARTESIAN_POINT('Ctrl Pts',(135.37268909646,-2.62078541903669,330.835940052673));
#53206=CARTESIAN_POINT('Ctrl Pts',(135.364931284937,-2.73580321778343,330.910579455236));
#53207=CARTESIAN_POINT('Ctrl Pts',(135.357173473415,-2.84758670154397,330.989958474069));
#53208=CARTESIAN_POINT('Ctrl Pts',(135.349421499892,-2.95928606468785,331.069277757673));
#53209=CARTESIAN_POINT('Ctrl Pts',(135.341669526369,-3.06775564004161,331.153329332784));
#53210=CARTESIAN_POINT('Ctrl Pts',(135.333917552846,-3.17257480817746,331.241815312013));
#53211=CARTESIAN_POINT('Ctrl Pts',(135.326168862289,-3.27734958533356,331.330263817378));
#53212=CARTESIAN_POINT('Ctrl Pts',(135.318420171731,-3.37847673199928,331.423142740093));
#53213=CARTESIAN_POINT('Ctrl Pts',(135.310671481173,-3.47556744244087,331.520112930633));
#53214=CARTESIAN_POINT('Ctrl Pts',(135.302924402796,-3.57263795234923,331.617062945715));
#53215=CARTESIAN_POINT('Ctrl Pts',(135.295177324418,-3.66567342009562,331.718102259436));
#53216=CARTESIAN_POINT('Ctrl Pts',(135.28743024604,-3.75432105973468,331.822854041292));
#53217=CARTESIAN_POINT('Ctrl Pts',(135.279683102734,-3.84296944232629,331.92760670107));
#53218=CARTESIAN_POINT('Ctrl Pts',(135.271935959428,-3.9272296709603,332.03607159267));
#53219=CARTESIAN_POINT('Ctrl Pts',(135.264188816122,-4.00678877075849,332.1478382218));
#53220=CARTESIAN_POINT('Ctrl Pts',(135.256439931094,-4.08636575713126,332.259629978441));
#53221=CARTESIAN_POINT('Ctrl Pts',(135.248691046066,-4.16123928489915,332.374724631333));
#53222=CARTESIAN_POINT('Ctrl Pts',(135.240942161038,-4.23113952223255,332.492682428191));
#53223=CARTESIAN_POINT('Ctrl Pts',(135.233185051264,-4.30111395240018,332.610765426674));
#53224=CARTESIAN_POINT('Ctrl Pts',(135.225427941489,-4.3661043478492,332.731717302955));
#53225=CARTESIAN_POINT('Ctrl Pts',(135.217670831714,-4.42588645068561,332.855072917757));
#53226=CARTESIAN_POINT('Ctrl Pts',(135.209909576788,-4.48570049916629,332.978494449857));
#53227=CARTESIAN_POINT('Ctrl Pts',(135.202148321862,-4.5403005538521,333.104321921533));
#53228=CARTESIAN_POINT('Ctrl Pts',(135.194387066936,-4.5895108149345,333.232070832273));
#53229=CARTESIAN_POINT('Ctrl Pts',(135.186613396531,-4.63879979639705,333.360024099638));
#53230=CARTESIAN_POINT('Ctrl Pts',(135.178839726126,-4.68268162994043,333.489904577677));
#53231=CARTESIAN_POINT('Ctrl Pts',(135.171066055722,-4.72103037537972,333.621212395892));
#53232=CARTESIAN_POINT('Ctrl Pts',(135.163654251545,-4.7575939774922,333.746407803576));
#53233=CARTESIAN_POINT('Ctrl Pts',(135.156242447368,-4.78912795969681,333.872900377318));
#53234=CARTESIAN_POINT('Ctrl Pts',(135.148830643191,-4.8155668746477,334.000250662268));
#53235=CARTESIAN_POINT('Ctrl Pts',(135.137812995018,-4.85486832623043,334.189556882562));
#53236=CARTESIAN_POINT('Ctrl Pts',(135.126795346845,-4.88301770679793,334.381251455537));
#53237=CARTESIAN_POINT('Ctrl Pts',(135.115777698672,-4.89978751616537,334.574247303086));
#53238=CARTESIAN_POINT('Ctrl Pts',(135.107790924617,-4.91194407410313,334.714151409988));
#53239=CARTESIAN_POINT('Ctrl Pts',(135.099804150563,-4.91812163449033,334.85473906561));
#53240=CARTESIAN_POINT('Ctrl Pts',(135.091817376508,-4.91824801995467,334.995586757208));
#53241=CARTESIAN_POINT('',(133.341817376552,-4.9182499977156,334.999850098394));
#53242=CARTESIAN_POINT('Ctrl Pts',(135.091817376461,-4.91824801995541,334.995586758035));
#53243=CARTESIAN_POINT('Ctrl Pts',(135.084167745614,-4.9183690703268,335.130488889871));
#53244=CARTESIAN_POINT('Ctrl Pts',(135.076518114767,-4.91293562494658,335.265568161034));
#53245=CARTESIAN_POINT('Ctrl Pts',(135.068868483919,-4.90193073749584,335.400322504106));
#53246=CARTESIAN_POINT('Ctrl Pts',(135.06122511569,-4.89093485955304,335.534966526165));
#53247=CARTESIAN_POINT('Ctrl Pts',(135.053581747462,-4.87437664553979,335.669285749588));
#53248=CARTESIAN_POINT('Ctrl Pts',(135.045938379233,-4.85229121336668,335.80277832755));
#53249=CARTESIAN_POINT('Ctrl Pts',(135.038298771281,-4.83021664647481,335.936205231706));
#53250=CARTESIAN_POINT('Ctrl Pts',(135.030659163329,-4.80262033353919,336.068805902345));
#53251=CARTESIAN_POINT('Ctrl Pts',(135.023019555377,-4.76958917031008,336.200084250776));
#53252=CARTESIAN_POINT('Ctrl Pts',(135.015381769418,-4.73656588477817,336.331331290256));
#53253=CARTESIAN_POINT('Ctrl Pts',(135.007743983458,-4.69811042400476,336.461256243887));
#53254=CARTESIAN_POINT('Ctrl Pts',(135.000106197498,-4.65436055645448,336.589374365284));
#53255=CARTESIAN_POINT('Ctrl Pts',(134.99246846978,-4.61061102251683,336.717491509721));
#53256=CARTESIAN_POINT('Ctrl Pts',(134.984830742062,-4.56156729253725,336.843801467951));
#53257=CARTESIAN_POINT('Ctrl Pts',(134.977193014344,-4.50741647584148,336.967836318349));
#53258=CARTESIAN_POINT('Ctrl Pts',(134.969553581374,-4.45325356905772,337.091898861631));
#53259=CARTESIAN_POINT('Ctrl Pts',(134.961914148403,-4.39398146988125,337.213684917937));
#53260=CARTESIAN_POINT('Ctrl Pts',(134.954274715433,-4.32983449128601,337.332748666396));
#53261=CARTESIAN_POINT('Ctrl Pts',(134.946627408995,-4.26562140056087,337.451935126137));
#53262=CARTESIAN_POINT('Ctrl Pts',(134.938980102556,-4.19652359055122,337.568393321046));
#53263=CARTESIAN_POINT('Ctrl Pts',(134.931332796118,-4.12282035733366,337.681703817288));
#53264=CARTESIAN_POINT('Ctrl Pts',(134.923681212767,-4.04907590407508,337.795077684743));
#53265=CARTESIAN_POINT('Ctrl Pts',(134.916029629416,-3.9707211331318,337.905300021115));
#53266=CARTESIAN_POINT('Ctrl Pts',(134.908378046065,-3.88807654125674,338.011983378412));
#53267=CARTESIAN_POINT('Ctrl Pts',(134.900715028075,-3.80530844407937,338.118826164898));
#53268=CARTESIAN_POINT('Ctrl Pts',(134.893052010084,-3.71823798485626,338.222119105096));
#53269=CARTESIAN_POINT('Ctrl Pts',(134.885388992094,-3.62722382843509,338.321510253022));
#53270=CARTESIAN_POINT('Ctrl Pts',(134.880456864368,-3.56864463093292,338.385481111109));
#53271=CARTESIAN_POINT('Ctrl Pts',(134.875524736642,-3.50843246631769,338.447836396263));
#53272=CARTESIAN_POINT('Ctrl Pts',(134.870592608916,-3.44669009985623,338.508491188254));
#53273=CARTESIAN_POINT('Ctrl Pts',(134.862817530138,-3.34935852413608,338.604108295562));
#53274=CARTESIAN_POINT('Ctrl Pts',(134.855042451359,-3.24789125660164,338.69582320963));
#53275=CARTESIAN_POINT('Ctrl Pts',(134.847267372581,-3.14263409442908,338.783257063832));
#53276=CARTESIAN_POINT('Ctrl Pts',(134.839501861532,-3.03750645789572,338.870583325109));
#53277=CARTESIAN_POINT('Ctrl Pts',(134.831736350483,-2.92859850396048,338.953638761191));
#53278=CARTESIAN_POINT('Ctrl Pts',(134.823970839434,-2.81629334282869,339.032080712193));
#53279=CARTESIAN_POINT('Ctrl Pts',(134.816213027912,-2.70409953259089,339.110444887772));
#53280=CARTESIAN_POINT('Ctrl Pts',(134.808455216389,-2.58851553672762,339.184204458973));
#53281=CARTESIAN_POINT('Ctrl Pts',(134.800697404867,-2.46995778728785,339.253056735046));
#53282=CARTESIAN_POINT('Ctrl Pts',(134.792945431344,-2.35148925631404,339.321857197597));
#53283=CARTESIAN_POINT('Ctrl Pts',(134.785193457821,-2.2300517627301,339.385757520038));
#53284=CARTESIAN_POINT('Ctrl Pts',(134.777441484298,-2.10609068775804,339.444498293108));
#53285=CARTESIAN_POINT('Ctrl Pts',(134.769692793741,-1.98218211037504,339.503214189425));
#53286=CARTESIAN_POINT('Ctrl Pts',(134.761944103183,-1.85575242973706,339.556774715293));
#53287=CARTESIAN_POINT('Ctrl Pts',(134.754195412625,-1.72727140112299,339.60496651121));
#53288=CARTESIAN_POINT('Ctrl Pts',(134.746448334247,-1.59881710406028,339.653148280421));
#53289=CARTESIAN_POINT('Ctrl Pts',(134.73870125587,-1.46831267370358,339.695963404303));
#53290=CARTESIAN_POINT('Ctrl Pts',(134.730954177492,-1.33624723745171,339.733246917593));
#53291=CARTESIAN_POINT('Ctrl Pts',(134.723207034186,-1.20418069436397,339.770530743354));
#53292=CARTESIAN_POINT('Ctrl Pts',(134.71545989088,-1.07055349545786,339.802282759856));
#53293=CARTESIAN_POINT('Ctrl Pts',(134.707712747574,-0.935868913327415,
339.828388182361));
#53294=CARTESIAN_POINT('Ctrl Pts',(134.699963862546,-0.80115405124334,339.85449947392));
#53295=CARTESIAN_POINT('Ctrl Pts',(134.692214977518,-0.665381716551916,
339.874961571007));
#53296=CARTESIAN_POINT('Ctrl Pts',(134.68446609249,-0.529063936707968,339.889711076677));
#53297=CARTESIAN_POINT('Ctrl Pts',(134.676708982715,-0.392601467764392,
339.904476237624));
#53298=CARTESIAN_POINT('Ctrl Pts',(134.66895187294,-0.255592786399069,339.913516652822));
#53299=CARTESIAN_POINT('Ctrl Pts',(134.661194763166,-0.118554144661556,
339.916820921824));
#53300=CARTESIAN_POINT('Ctrl Pts',(134.65343350824,0.0185577261445966,339.920126956521));
#53301=CARTESIAN_POINT('Ctrl Pts',(134.645672253313,0.155699198609651,339.917690744246));
#53302=CARTESIAN_POINT('Ctrl Pts',(134.637910998387,0.292356475275361,339.909553009579));
#53303=CARTESIAN_POINT('Ctrl Pts',(134.630137327982,0.429232359047048,339.901402257188));
#53304=CARTESIAN_POINT('Ctrl Pts',(134.622363657578,0.565622110155068,339.887531796357));
#53305=CARTESIAN_POINT('Ctrl Pts',(134.614589987173,0.701018598987366,339.868034098727));
#53306=CARTESIAN_POINT('Ctrl Pts',(134.607178182996,0.830112348688905,339.849444023613));
#53307=CARTESIAN_POINT('Ctrl Pts',(134.599766378819,0.958302944793477,339.825738869831));
#53308=CARTESIAN_POINT('Ctrl Pts',(134.592354574642,1.085163306511,339.797041136024));
#53309=CARTESIAN_POINT('Ctrl Pts',(134.584579495864,1.21824147245513,339.766936840795));
#53310=CARTESIAN_POINT('Ctrl Pts',(134.576804417085,1.35027626100033,339.731243053419));
#53311=CARTESIAN_POINT('Ctrl Pts',(134.569029338307,1.48076194442432,339.690045535647));
#53312=CARTESIAN_POINT('Ctrl Pts',(134.561263827258,1.61108705690768,339.648898714044));
#53313=CARTESIAN_POINT('Ctrl Pts',(134.553498316209,1.73986648803078,339.602261754314));
#53314=CARTESIAN_POINT('Ctrl Pts',(134.54573280516,1.86660476487117,339.550271389078));
#53315=CARTESIAN_POINT('Ctrl Pts',(134.537974993637,1.99321738034113,339.49833257244));
#53316=CARTESIAN_POINT('Ctrl Pts',(134.530217182115,2.11779250972559,339.441051060743));
#53317=CARTESIAN_POINT('Ctrl Pts',(134.522459370593,2.23985025863769,339.378613237245));
#53318=CARTESIAN_POINT('Ctrl Pts',(134.51470739707,2.36181615522302,339.31622240019));
#53319=CARTESIAN_POINT('Ctrl Pts',(134.506955423547,2.48126809547787,339.248683152153));
#53320=CARTESIAN_POINT('Ctrl Pts',(134.499203450024,2.5977469152836,339.176229642469));
#53321=CARTESIAN_POINT('Ctrl Pts',(134.491454759466,2.71417640623994,339.103806816888));
#53322=CARTESIAN_POINT('Ctrl Pts',(134.483706068909,2.82763494983268,339.02647407503));
#53323=CARTESIAN_POINT('Ctrl Pts',(134.475957378351,2.93768891596891,338.944510983062));
#53324=CARTESIAN_POINT('Ctrl Pts',(134.468210299973,3.04771998445822,338.862564944199));
#53325=CARTESIAN_POINT('Ctrl Pts',(134.460463221595,3.15434757116053,338.775990704786));
#53326=CARTESIAN_POINT('Ctrl Pts',(134.452716143218,3.25716825836363,338.685110310317));
#53327=CARTESIAN_POINT('Ctrl Pts',(134.444968999912,3.35998980730299,338.594229154184));
#53328=CARTESIAN_POINT('Ctrl Pts',(134.437221856606,3.45900410023385,338.499042029872));
#53329=CARTESIAN_POINT('Ctrl Pts',(134.4294747133,3.55384226254359,338.399910033436));
#53330=CARTESIAN_POINT('Ctrl Pts',(134.421725828272,3.64870174648582,338.300755750022));
#53331=CARTESIAN_POINT('Ctrl Pts',(134.413976943244,3.73938296138243,338.197655112053));
#53332=CARTESIAN_POINT('Ctrl Pts',(134.406228058216,3.82555550795274,338.091004386615));
#53333=CARTESIAN_POINT('Ctrl Pts',(134.398470948441,3.91181951895428,337.984240460994));
#53334=CARTESIAN_POINT('Ctrl Pts',(134.390713838666,3.99356505600683,337.873919225285));
#53335=CARTESIAN_POINT('Ctrl Pts',(134.382956728892,4.07050315862327,337.760468637412));
#53336=CARTESIAN_POINT('Ctrl Pts',(134.375195473966,4.14748237450166,337.646957425173));
#53337=CARTESIAN_POINT('Ctrl Pts',(134.367434219039,4.21964883155236,337.530313860941));
#53338=CARTESIAN_POINT('Ctrl Pts',(134.359672964113,4.28675873065632,337.410992046366));
#53339=CARTESIAN_POINT('Ctrl Pts',(134.351899293709,4.35397598372786,337.291479355775));
#53340=CARTESIAN_POINT('Ctrl Pts',(134.344125623304,4.41612033766883,337.169280202078));
#53341=CARTESIAN_POINT('Ctrl Pts',(134.336351952899,4.47299511692283,337.044871083097));
#53342=CARTESIAN_POINT('Ctrl Pts',(134.328940148722,4.52722236151892,336.926253238535));
#53343=CARTESIAN_POINT('Ctrl Pts',(134.321528344545,4.57665947910355,336.805626812531));
#53344=CARTESIAN_POINT('Ctrl Pts',(134.314116540368,4.62117836347678,336.683417237477));
#53345=CARTESIAN_POINT('Ctrl Pts',(134.30634146159,4.66787925098841,336.555217807104));
#53346=CARTESIAN_POINT('Ctrl Pts',(134.298566382811,4.70931518392665,336.42487098012));
#53347=CARTESIAN_POINT('Ctrl Pts',(134.290791304033,4.74528460288934,336.292848444359));
#53348=CARTESIAN_POINT('Ctrl Pts',(134.283025792984,4.7812097591921,336.160988370733));
#53349=CARTESIAN_POINT('Ctrl Pts',(134.275260281935,4.81168168434252,336.027457064775));
#53350=CARTESIAN_POINT('Ctrl Pts',(134.267494770886,4.83654723088881,335.892745174102));
#53351=CARTESIAN_POINT('Ctrl Pts',(134.259736959363,4.86138812317328,335.75816685066));
#53352=CARTESIAN_POINT('Ctrl Pts',(134.251979147841,4.88063362856871,335.622410653875));
#53353=CARTESIAN_POINT('Ctrl Pts',(134.244221336319,4.89418078234591,335.485980999851));
#53354=CARTESIAN_POINT('Ctrl Pts',(134.236469362796,4.90771774146024,335.349654013468));
#53355=CARTESIAN_POINT('Ctrl Pts',(134.228717389273,4.91556484592206,335.212654965999));
#53356=CARTESIAN_POINT('Ctrl Pts',(134.22096541575,4.91767051685054,335.075496689986));
#53357=CARTESIAN_POINT('Ctrl Pts',(134.213216725192,4.91977529602614,334.938396500585));
#53358=CARTESIAN_POINT('Ctrl Pts',(134.205468034635,4.91614347176402,334.801137606774));
#53359=CARTESIAN_POINT('Ctrl Pts',(134.197719344077,4.90677547509316,334.664235946647));
#53360=CARTESIAN_POINT('Ctrl Pts',(134.189972265699,4.89740942751224,334.527362770052));
#53361=CARTESIAN_POINT('Ctrl Pts',(134.182225187322,4.88230960806394,334.390847069019));
#53362=CARTESIAN_POINT('Ctrl Pts',(134.174478108944,4.8615285192027,334.255202363404));
#53363=CARTESIAN_POINT('Ctrl Pts',(134.166730965638,4.84074725617597,334.119556520956));
#53364=CARTESIAN_POINT('Ctrl Pts',(134.158983822332,4.81428468795787,333.984782074852));
#53365=CARTESIAN_POINT('Ctrl Pts',(134.151236679026,4.78224484870461,333.851384629418));
#53366=CARTESIAN_POINT('Ctrl Pts',(134.143487793998,4.75019780621522,333.717957193405));
#53367=CARTESIAN_POINT('Ctrl Pts',(134.13573890897,4.71257108885928,333.585907754082));
#53368=CARTESIAN_POINT('Ctrl Pts',(134.127990023942,4.6695191280734,333.455728594108));
#53369=CARTESIAN_POINT('Ctrl Pts',(134.120232914167,4.62642147149155,333.325411260628));
#53370=CARTESIAN_POINT('Ctrl Pts',(134.112475804392,4.57788719144039,333.196968543683));
#53371=CARTESIAN_POINT('Ctrl Pts',(134.104718694618,4.52411979376921,333.070875028899));
#53372=CARTESIAN_POINT('Ctrl Pts',(134.096957439692,4.47032366451993,332.944714133773));
#53373=CARTESIAN_POINT('Ctrl Pts',(134.089196184765,4.41128901369633,332.820905294822));
#53374=CARTESIAN_POINT('Ctrl Pts',(134.081434929839,4.34726577137163,332.699899268388));
#53375=CARTESIAN_POINT('Ctrl Pts',(134.073661259435,4.28314011272427,332.578699671748));
#53376=CARTESIAN_POINT('Ctrl Pts',(134.06588758903,4.21401011313568,332.460312184876));
#53377=CARTESIAN_POINT('Ctrl Pts',(134.058113918625,4.14017003736031,332.345160056756));
#53378=CARTESIAN_POINT('Ctrl Pts',(134.050702114448,4.06976723487698,332.235368287904));
#53379=CARTESIAN_POINT('Ctrl Pts',(134.043290310271,3.99508316082387,332.128517680378));
#53380=CARTESIAN_POINT('Ctrl Pts',(134.035878506094,3.91640624476005,332.024946187293));
#53381=CARTESIAN_POINT('Ctrl Pts',(134.028103427315,3.83387313867383,331.916298346808));
#53382=CARTESIAN_POINT('Ctrl Pts',(134.020328348537,3.74668507194117,331.810915839423));
#53383=CARTESIAN_POINT('Ctrl Pts',(134.012553269759,3.65512962156838,331.709223418092));
#53384=CARTESIAN_POINT('Ctrl Pts',(134.00478775871,3.56368683600598,331.60765613576));
#53385=CARTESIAN_POINT('Ctrl Pts',(133.997022247661,3.46788761923814,331.509770192132));
#53386=CARTESIAN_POINT('Ctrl Pts',(133.989256736612,3.36806169043975,331.415959889748));
#53387=CARTESIAN_POINT('Ctrl Pts',(133.981498925089,3.26833473934002,331.322242600552));
#53388=CARTESIAN_POINT('Ctrl Pts',(133.973741113567,3.16458930450799,331.232593176711));
#53389=CARTESIAN_POINT('Ctrl Pts',(133.965983302045,3.05719384008437,331.147371171959));
#53390=CARTESIAN_POINT('Ctrl Pts',(133.958231328522,2.94987919415438,331.06221329947));
#53391=CARTESIAN_POINT('Ctrl Pts',(133.950479354999,2.83892029088234,330.981476456328));
#53392=CARTESIAN_POINT('Ctrl Pts',(133.942727381476,2.72472046980289,330.905481539431));
#53393=CARTESIAN_POINT('Ctrl Pts',(133.934978690918,2.6105690124148,330.829518806427));
#53394=CARTESIAN_POINT('Ctrl Pts',(133.927230000361,2.49317969181753,330.758294221576));
#53395=CARTESIAN_POINT('Ctrl Pts',(133.919481309803,2.37298660461303,330.692086626123));
#53396=CARTESIAN_POINT('Ctrl Pts',(133.911734231425,2.25281852458419,330.625892805714));
#53397=CARTESIAN_POINT('Ctrl Pts',(133.903987153047,2.12984818041996,330.56471408693));
#53398=CARTESIAN_POINT('Ctrl Pts',(133.89624007467,2.00453581401394,330.508784214399));
#53399=CARTESIAN_POINT('Ctrl Pts',(133.888492931364,1.87922239736976,330.452853873121));
#53400=CARTESIAN_POINT('Ctrl Pts',(133.880745788058,1.75156727626953,330.402172625147));
#53401=CARTESIAN_POINT('Ctrl Pts',(133.872998644752,1.62205192302869,330.356926597447));
#53402=CARTESIAN_POINT('Ctrl Pts',(133.865249759724,1.49250745198675,330.311670397479));
#53403=CARTESIAN_POINT('Ctrl Pts',(133.857500874696,1.36110228552649,330.271851978221));
#53404=CARTESIAN_POINT('Ctrl Pts',(133.849751989668,1.22833396635186,330.237607877379));
#53405=CARTESIAN_POINT('Ctrl Pts',(133.841994879893,1.09542472551155,330.203327429494));
#53406=CARTESIAN_POINT('Ctrl Pts',(133.834237770119,0.961149820794958,330.174633216842));
#53407=CARTESIAN_POINT('Ctrl Pts',(133.826480660344,0.826018470073655,330.151610932526));
#53408=CARTESIAN_POINT('Ctrl Pts',(133.818719405418,0.690814909479144,330.128576345839));
#53409=CARTESIAN_POINT('Ctrl Pts',(133.810958150491,0.554754378491972,330.11121977626));
#53410=CARTESIAN_POINT('Ctrl Pts',(133.803196895565,0.418351179238423,330.099574982379));
#53411=CARTESIAN_POINT('Ctrl Pts',(133.795423225161,0.281729779319628,330.087911560622));
#53412=CARTESIAN_POINT('Ctrl Pts',(133.787649554756,0.144765006466774,330.081978189881));
#53413=CARTESIAN_POINT('Ctrl Pts',(133.779875884351,0.00797202332331137,
330.081756460956));
#53414=CARTESIAN_POINT('Ctrl Pts',(133.772464080174,-0.122453213544662,
330.081545053566));
#53415=CARTESIAN_POINT('Ctrl Pts',(133.765052275997,-0.252722006812522,
330.086525489933));
#53416=CARTESIAN_POINT('Ctrl Pts',(133.75764047182,-0.382394078711341,330.09663810931));
#53417=CARTESIAN_POINT('Ctrl Pts',(133.749865393042,-0.518421765126657,
330.107246378287));
#53418=CARTESIAN_POINT('Ctrl Pts',(133.742090314263,-0.654222629583345,
330.123536162085));
#53419=CARTESIAN_POINT('Ctrl Pts',(133.734315235485,-0.789283863840687,
330.145495489261));
#53420=CARTESIAN_POINT('Ctrl Pts',(133.726549724436,-0.924178896651132,
330.167427794088));
#53421=CARTESIAN_POINT('Ctrl Pts',(133.718784213387,-1.05833572810374,330.195015698463));
#53422=CARTESIAN_POINT('Ctrl Pts',(133.711018702338,-1.19124435081706,330.228195314229));
#53423=CARTESIAN_POINT('Ctrl Pts',(133.703260890815,-1.32402119424423,330.261342032309));
#53424=CARTESIAN_POINT('Ctrl Pts',(133.695503079293,-1.45555191503853,330.300069334448));
#53425=CARTESIAN_POINT('Ctrl Pts',(133.687745267771,-1.58533476511591,330.344261954855));
#53426=CARTESIAN_POINT('Ctrl Pts',(133.679993294248,-1.71501994948217,330.388421318913));
#53427=CARTESIAN_POINT('Ctrl Pts',(133.672241320725,-1.84295951270638,330.438037689376));
#53428=CARTESIAN_POINT('Ctrl Pts',(133.664489347202,-1.96866533557613,330.492945545148));
#53429=CARTESIAN_POINT('Ctrl Pts',(133.656740656644,-2.09431792195539,330.547830147411));
#53430=CARTESIAN_POINT('Ctrl Pts',(133.648991966087,-2.21773829203901,330.608001621764));
#53431=CARTESIAN_POINT('Ctrl Pts',(133.641243275529,-2.33845704769644,330.67324582411));
#53432=CARTESIAN_POINT('Ctrl Pts',(133.633496197151,-2.45915068680881,330.738476451856));
#53433=CARTESIAN_POINT('Ctrl Pts',(133.625749118773,-2.57714348588889,330.808777522553));
#53434=CARTESIAN_POINT('Ctrl Pts',(133.618002040396,-2.69198982079654,330.883888501604));
#53435=CARTESIAN_POINT('Ctrl Pts',(133.61025489709,-2.80683711822673,330.959000110157));
#53436=CARTESIAN_POINT('Ctrl Pts',(133.602507753784,-2.91853757176185,331.038921493524));
#53437=CARTESIAN_POINT('Ctrl Pts',(133.594760610478,-3.02667411096457,331.123348495348));
#53438=CARTESIAN_POINT('Ctrl Pts',(133.58701172545,-3.13483496155682,331.207794478155));
#53439=CARTESIAN_POINT('Ctrl Pts',(133.579262840422,-3.23942999539763,331.296747854596));
#53440=CARTESIAN_POINT('Ctrl Pts',(133.571513955394,-3.3400751461114,331.389864118786));
#53441=CARTESIAN_POINT('Ctrl Pts',(133.563756845619,-3.44082712262855,331.483079217541));
#53442=CARTESIAN_POINT('Ctrl Pts',(133.555999735845,-3.53762055384682,331.580465764607));
#53443=CARTESIAN_POINT('Ctrl Pts',(133.54824262607,-3.63010781159711,331.681641921269));
#53444=CARTESIAN_POINT('Ctrl Pts',(133.540481371144,-3.72264449158048,331.782872143233));
#53445=CARTESIAN_POINT('Ctrl Pts',(133.532720116218,-3.81087016169437,331.887895710745));
#53446=CARTESIAN_POINT('Ctrl Pts',(133.524958861291,-3.89447811522964,331.996298404885));
#53447=CARTESIAN_POINT('Ctrl Pts',(133.517185190887,-3.97821981424292,332.104874508007));
#53448=CARTESIAN_POINT('Ctrl Pts',(133.509411520482,-4.05732880990968,332.216840220149));
#53449=CARTESIAN_POINT('Ctrl Pts',(133.501637850077,-4.13154179885157,332.331752367781));
#53450=CARTESIAN_POINT('Ctrl Pts',(133.4942260459,-4.20230015530368,332.441315327294));
#53451=CARTESIAN_POINT('Ctrl Pts',(133.486814241723,-4.26860791896853,332.553556334611));
#53452=CARTESIAN_POINT('Ctrl Pts',(133.479402437546,-4.33027700027737,332.66807286491));
#53453=CARTESIAN_POINT('Ctrl Pts',(133.471206716576,-4.39846857291137,332.794701349199));
#53454=CARTESIAN_POINT('Ctrl Pts',(133.463010995606,-4.46118481695896,332.924476920584));
#53455=CARTESIAN_POINT('Ctrl Pts',(133.454815274636,-4.51814030822212,333.056911937735));
#53456=CARTESIAN_POINT('Ctrl Pts',(133.44663396167,-4.57499567224022,333.189114135307));
#53457=CARTESIAN_POINT('Ctrl Pts',(133.438452648704,-4.62611033588138,333.323966161439));
#53458=CARTESIAN_POINT('Ctrl Pts',(133.430271335738,-4.67124452783009,333.460955613467));
#53459=CARTESIAN_POINT('Ctrl Pts',(133.42210923541,-4.71627272861936,333.597623365467));
#53460=CARTESIAN_POINT('Ctrl Pts',(133.413947135081,-4.75534836193544,333.736418222766));
#53461=CARTESIAN_POINT('Ctrl Pts',(133.405785034752,-4.78827983031108,333.876808418329));
#53462=CARTESIAN_POINT('Ctrl Pts',(133.397634429049,-4.82116492154199,334.017000903412));
#53463=CARTESIAN_POINT('Ctrl Pts',(133.389483823346,-4.84792301213026,334.158783932328));
#53464=CARTESIAN_POINT('Ctrl Pts',(133.381333217643,-4.86841183606882,334.30160952403));
#53465=CARTESIAN_POINT('Ctrl Pts',(133.373197820997,-4.8888624277958,334.444168602718));
#53466=CARTESIAN_POINT('Ctrl Pts',(133.36506242435,-4.90306703361276,334.587766040657));
#53467=CARTESIAN_POINT('Ctrl Pts',(133.356927027704,-4.91093422629604,334.731843166236));
#53468=CARTESIAN_POINT('Ctrl Pts',(133.35189047732,-4.91580473403529,334.821040009816));
#53469=CARTESIAN_POINT('Ctrl Pts',(133.346853926936,-4.91824727202096,334.910420451796));
#53470=CARTESIAN_POINT('Ctrl Pts',(133.341817376552,-4.9182499977156,334.999850098394));
#53471=CARTESIAN_POINT('',(131.591817376536,-4.91824796507461,335.004473984742));
#53472=CARTESIAN_POINT('Ctrl Pts',(133.341817376508,-4.91824999771563,334.99985009918));
#53473=CARTESIAN_POINT('Ctrl Pts',(133.333720689468,-4.91825437948074,335.143615932019));
#53474=CARTESIAN_POINT('Ctrl Pts',(133.325624002429,-4.91195079819547,335.287266411861));
#53475=CARTESIAN_POINT('Ctrl Pts',(133.317527315389,-4.89939538494284,335.430241704744));
#53476=CARTESIAN_POINT('Ctrl Pts',(133.309420634577,-4.88682447449389,335.573393472597));
#53477=CARTESIAN_POINT('Ctrl Pts',(133.301313953765,-4.86798636506514,335.715868055862));
#53478=CARTESIAN_POINT('Ctrl Pts',(133.293207272952,-4.84298863388882,335.857113851553));
#53479=CARTESIAN_POINT('Ctrl Pts',(133.285082101954,-4.81793388644398,335.998681808809));
#53480=CARTESIAN_POINT('Ctrl Pts',(133.276956930956,-4.78669148748155,336.139015042695));
#53481=CARTESIAN_POINT('Ctrl Pts',(133.268831759958,-4.74941987798039,336.277573436302));
#53482=CARTESIAN_POINT('Ctrl Pts',(133.260696913547,-4.71210388563228,336.416296824554));
#53483=CARTESIAN_POINT('Ctrl Pts',(133.252562067136,-4.66874445716667,336.553240834597));
#53484=CARTESIAN_POINT('Ctrl Pts',(133.244427220724,-4.61954894920918,336.687883458169));
#53485=CARTESIAN_POINT('Ctrl Pts',(133.236273866015,-4.57024151226322,336.82283241891));
#53486=CARTESIAN_POINT('Ctrl Pts',(133.228120511306,-4.51507157414448,336.955469211743));
#53487=CARTESIAN_POINT('Ctrl Pts',(133.219967156596,-4.45429415459308,337.085292940298));
#53488=CARTESIAN_POINT('Ctrl Pts',(133.213699572155,-4.40757380171516,337.185090043479));
#53489=CARTESIAN_POINT('Ctrl Pts',(133.207431987714,-4.3575408460764,337.283225320956));
#53490=CARTESIAN_POINT('Ctrl Pts',(133.201164403272,-4.30432863347267,337.379482733194));
#53491=CARTESIAN_POINT('Ctrl Pts',(133.193389324494,-4.23831769275951,337.498892207476));
#53492=CARTESIAN_POINT('Ctrl Pts',(133.185614245716,-4.16722974095943,337.615741404958));
#53493=CARTESIAN_POINT('Ctrl Pts',(133.177839166937,-4.09128812889158,337.72956855728));
#53494=CARTESIAN_POINT('Ctrl Pts',(133.170073655888,-4.01543996781198,337.843255638044));
#53495=CARTESIAN_POINT('Ctrl Pts',(133.162308144839,-3.93475024535724,337.953927750988));
#53496=CARTESIAN_POINT('Ctrl Pts',(133.15454263379,-3.84948840351955,338.061147185888));
#53497=CARTESIAN_POINT('Ctrl Pts',(133.146784822268,-3.76431109904648,338.168260312406));
#53498=CARTESIAN_POINT('Ctrl Pts',(133.139027010746,-3.67457093836872,338.271927269557));
#53499=CARTESIAN_POINT('Ctrl Pts',(133.131269199224,-3.58058070259055,338.371739149866));
#53500=CARTESIAN_POINT('Ctrl Pts',(133.123517225701,-3.48666119744514,338.47147591857));
#53501=CARTESIAN_POINT('Ctrl Pts',(133.115765252178,-3.38849825017902,338.567363101447));
#53502=CARTESIAN_POINT('Ctrl Pts',(133.108013278655,-3.28644473493321,338.659025015866));
#53503=CARTESIAN_POINT('Ctrl Pts',(133.100264588097,-3.1844344394118,338.750648111409));
#53504=CARTESIAN_POINT('Ctrl Pts',(133.09251589754,-3.07853714317919,338.838049236849));
#53505=CARTESIAN_POINT('Ctrl Pts',(133.084767206982,-2.96914221809585,338.920889892769));
#53506=CARTESIAN_POINT('Ctrl Pts',(133.077020128604,-2.85977005354035,339.003713313));
#53507=CARTESIAN_POINT('Ctrl Pts',(133.069273050226,-2.74690201901675,339.081977915207));
#53508=CARTESIAN_POINT('Ctrl Pts',(133.061525971848,-2.6309598588071,339.155386057137));
#53509=CARTESIAN_POINT('Ctrl Pts',(133.053778828543,-2.5150167268906,339.228794814297));
#53510=CARTESIAN_POINT('Ctrl Pts',(133.046031685237,-2.39599974814581,339.297346820904));
#53511=CARTESIAN_POINT('Ctrl Pts',(133.038284541931,-2.27435853910797,339.360788494996));
#53512=CARTESIAN_POINT('Ctrl Pts',(133.030535656903,-2.15268998254395,339.424244432123));
#53513=CARTESIAN_POINT('Ctrl Pts',(133.022786771875,-2.02839636818998,339.482587569812));
#53514=CARTESIAN_POINT('Ctrl Pts',(133.015037886847,-1.90195036286914,339.535611081175));
#53515=CARTESIAN_POINT('Ctrl Pts',(133.007280777072,-1.77537014645164,339.588690872242));
#53516=CARTESIAN_POINT('Ctrl Pts',(132.999523667297,-1.64663333645803,339.636439606561));
#53517=CARTESIAN_POINT('Ctrl Pts',(132.991766557523,-1.51623148161709,339.678699088064));
#53518=CARTESIAN_POINT('Ctrl Pts',(132.984005302597,-1.38575994419436,339.720981151683));
#53519=CARTESIAN_POINT('Ctrl Pts',(132.97624404767,-1.25362196538693,339.757768012881));
#53520=CARTESIAN_POINT('Ctrl Pts',(132.968482792744,-1.12032161084018,339.788952134944));
#53521=CARTESIAN_POINT('Ctrl Pts',(132.96070912234,-0.986808019168632,339.82018614144));
#53522=CARTESIAN_POINT('Ctrl Pts',(132.952935451935,-0.852128720274987,
339.845799425893));
#53523=CARTESIAN_POINT('Ctrl Pts',(132.94516178153,-0.716796150713376,339.865735950586));
#53524=CARTESIAN_POINT('Ctrl Pts',(132.937749977353,-0.587763344823718,
339.884744425258));
#53525=CARTESIAN_POINT('Ctrl Pts',(132.930338173176,-0.458137005228234,
339.898592722226));
#53526=CARTESIAN_POINT('Ctrl Pts',(132.922926368999,-0.328361411517108,
339.907276418333));
#53527=CARTESIAN_POINT('Ctrl Pts',(132.915151290221,-0.192225129376943,
339.916385728254));
#53528=CARTESIAN_POINT('Ctrl Pts',(132.907376211442,-0.0554943766009946,
339.919840158553));
#53529=CARTESIAN_POINT('Ctrl Pts',(132.899601132664,0.0813216680008721,
339.917577640344));
#53530=CARTESIAN_POINT('Ctrl Pts',(132.891835621615,0.217969351749859,339.915317906308));
#53531=CARTESIAN_POINT('Ctrl Pts',(132.884070110566,0.354701731405614,339.907355227934));
#53532=CARTESIAN_POINT('Ctrl Pts',(132.876304599517,0.491004916581289,339.893679314625));
#53533=CARTESIAN_POINT('Ctrl Pts',(132.868546787994,0.627172956751564,339.880016961025));
#53534=CARTESIAN_POINT('Ctrl Pts',(132.860788976472,0.762912262889284,339.860652684312));
#53535=CARTESIAN_POINT('Ctrl Pts',(132.85303116495,0.897709712172195,339.835628225492));
#53536=CARTESIAN_POINT('Ctrl Pts',(132.845279191427,1.0324057221004,339.810622598371));
#53537=CARTESIAN_POINT('Ctrl Pts',(132.837527217904,1.16616090319948,339.77996533846));
#53538=CARTESIAN_POINT('Ctrl Pts',(132.829775244381,1.29846837548461,339.743749881725));
#53539=CARTESIAN_POINT('Ctrl Pts',(132.822026553823,1.43071981547639,339.707549762258));
#53540=CARTESIAN_POINT('Ctrl Pts',(132.814277863266,1.56152438985654,339.665796230687));
#53541=CARTESIAN_POINT('Ctrl Pts',(132.806529172708,1.69038673579029,339.61863353666));
#53542=CARTESIAN_POINT('Ctrl Pts',(132.79878209433,1.81922227083668,339.571480655226));
#53543=CARTESIAN_POINT('Ctrl Pts',(132.791035015953,1.94611601438184,339.518920984138));
#53544=CARTESIAN_POINT('Ctrl Pts',(132.783287937575,2.07058944267369,339.461148105857));
#53545=CARTESIAN_POINT('Ctrl Pts',(132.775540794269,2.19506391417259,339.403374743383));
#53546=CARTESIAN_POINT('Ctrl Pts',(132.767793650963,2.31711767541261,339.340388251129));
#53547=CARTESIAN_POINT('Ctrl Pts',(132.760046507657,2.43629417060654,339.272429493481));
#53548=CARTESIAN_POINT('Ctrl Pts',(132.752297622629,2.55549745920697,339.204455457262));
#53549=CARTESIAN_POINT('Ctrl Pts',(132.744548737601,2.67182185507944,339.131507124796));
#53550=CARTESIAN_POINT('Ctrl Pts',(132.736799852573,2.78483764594164,339.053870045801));
#53551=CARTESIAN_POINT('Ctrl Pts',(132.729042742798,2.89797339293189,338.976150562009));
#53552=CARTESIAN_POINT('Ctrl Pts',(132.721285633024,3.00779319709961,338.893732611968));
#53553=CARTESIAN_POINT('Ctrl Pts',(132.713528523249,3.11389802277347,338.806943940521));
#53554=CARTESIAN_POINT('Ctrl Pts',(132.705767268323,3.22005954747363,338.720108891982));
#53555=CARTESIAN_POINT('Ctrl Pts',(132.698006013397,3.32250184627625,338.628898727987));
#53556=CARTESIAN_POINT('Ctrl Pts',(132.69024475847,3.42086171042138,338.533679133803));
#53557=CARTESIAN_POINT('Ctrl Pts',(132.682471088066,3.51937891829367,338.4383072193));
#53558=CARTESIAN_POINT('Ctrl Pts',(132.674697417661,3.61380037215368,338.338913341511));
#53559=CARTESIAN_POINT('Ctrl Pts',(132.666923747256,3.70380163986602,338.235898094042));
#53560=CARTESIAN_POINT('Ctrl Pts',(132.659511943079,3.78961332691325,338.137678231127));
#53561=CARTESIAN_POINT('Ctrl Pts',(132.652100138902,3.87140690558669,338.036166784809));
#53562=CARTESIAN_POINT('Ctrl Pts',(132.644688334725,3.94893823118078,337.931734965651));
#53563=CARTESIAN_POINT('Ctrl Pts',(132.636913255947,4.03026959799639,337.822184631949));
#53564=CARTESIAN_POINT('Ctrl Pts',(132.629138177168,4.10716735806855,337.709074215367));
#53565=CARTESIAN_POINT('Ctrl Pts',(132.62136309839,4.17930377047498,337.592798306192));
#53566=CARTESIAN_POINT('Ctrl Pts',(132.613597587341,4.25135141443341,337.476665481927));
#53567=CARTESIAN_POINT('Ctrl Pts',(132.605832076292,4.31864916464669,337.35737524465));
#53568=CARTESIAN_POINT('Ctrl Pts',(132.598066565243,4.38091027195633,337.23535416692));
#53569=CARTESIAN_POINT('Ctrl Pts',(132.59030875372,4.44310964719692,337.113454073444));
#53570=CARTESIAN_POINT('Ctrl Pts',(132.582550942198,4.50028214106122,336.988828873789));
#53571=CARTESIAN_POINT('Ctrl Pts',(132.574793130676,4.55218517424933,336.861932652339));
#53572=CARTESIAN_POINT('Ctrl Pts',(132.567041157153,4.60404914875895,336.735131924319));
#53573=CARTESIAN_POINT('Ctrl Pts',(132.55928918363,4.65065140821951,336.60606393654));
#53574=CARTESIAN_POINT('Ctrl Pts',(132.551537210107,4.69179622308286,336.475205498758));
#53575=CARTESIAN_POINT('Ctrl Pts',(132.543788519549,4.73292361309269,336.344402479602));
#53576=CARTESIAN_POINT('Ctrl Pts',(132.536039828992,4.76859803838411,336.211810890662));
#53577=CARTESIAN_POINT('Ctrl Pts',(132.528291138434,4.79867273231001,336.077925354876));
#53578=CARTESIAN_POINT('Ctrl Pts',(132.520544060056,4.82874116894465,335.944067675094));
#53579=CARTESIAN_POINT('Ctrl Pts',(132.512796981678,4.85321210600861,335.808916965088));
#53580=CARTESIAN_POINT('Ctrl Pts',(132.505049903301,4.87198937446404,335.672980384268));
#53581=CARTESIAN_POINT('Ctrl Pts',(132.497302759995,4.89076680029106,335.537042664169));
#53582=CARTESIAN_POINT('Ctrl Pts',(132.489555616689,4.90385040884697,335.400319447316));
#53583=CARTESIAN_POINT('Ctrl Pts',(132.481808473383,4.91119567959973,335.263325006752));
#53584=CARTESIAN_POINT('Ctrl Pts',(132.474059588355,4.91854260172529,335.12629976693));
#53585=CARTESIAN_POINT('Ctrl Pts',(132.466310703327,4.92014859796904,334.989003572297));
#53586=CARTESIAN_POINT('Ctrl Pts',(132.458561818299,4.91602125120837,334.851952304416));
#53587=CARTESIAN_POINT('Ctrl Pts',(132.450804708524,4.91188952363919,334.714755568904));
#53588=CARTESIAN_POINT('Ctrl Pts',(132.443047598749,4.9020123086338,334.577804670768));
#53589=CARTESIAN_POINT('Ctrl Pts',(132.435290488975,4.88644927272418,334.441612529158));
#53590=CARTESIAN_POINT('Ctrl Pts',(132.427529234048,4.87087792042578,334.305347610822));
#53591=CARTESIAN_POINT('Ctrl Pts',(132.419767979122,4.84961475365808,334.169842642872));
#53592=CARTESIAN_POINT('Ctrl Pts',(132.412006724196,4.82277073186459,334.035600948585));
#53593=CARTESIAN_POINT('Ctrl Pts',(132.404233053791,4.79588376838469,333.901144511336));
#53594=CARTESIAN_POINT('Ctrl Pts',(132.396459383387,4.76339820266194,333.7679557659));
#53595=CARTESIAN_POINT('Ctrl Pts',(132.388685712982,4.72547533356174,333.636524318369));
#53596=CARTESIAN_POINT('Ctrl Pts',(132.381273908805,4.68931778314214,333.511211036341));
#53597=CARTESIAN_POINT('Ctrl Pts',(132.373862104628,4.64821784101662,333.387495402718));
#53598=CARTESIAN_POINT('Ctrl Pts',(132.366450300451,4.60235554535699,333.265783607325));
#53599=CARTESIAN_POINT('Ctrl Pts',(132.358675221672,4.55424540197007,333.138106354279));
#53600=CARTESIAN_POINT('Ctrl Pts',(132.350900142894,4.50074222992901,333.012230850606));
#53601=CARTESIAN_POINT('Ctrl Pts',(132.343125064116,4.4420004892061,332.888646236086));
#53602=CARTESIAN_POINT('Ctrl Pts',(132.335359553067,4.38333103393465,332.765213700302));
#53603=CARTESIAN_POINT('Ctrl Pts',(132.327594042018,4.31943600264773,332.64406679415));
#53604=CARTESIAN_POINT('Ctrl Pts',(132.319828530968,4.25051893288553,332.525677494003));
#53605=CARTESIAN_POINT('Ctrl Pts',(132.312070719446,4.18167019459909,332.407405577193));
#53606=CARTESIAN_POINT('Ctrl Pts',(132.304312907924,4.10780952243509,332.291886160856));
#53607=CARTESIAN_POINT('Ctrl Pts',(132.296555096402,4.02918749205899,332.179568966215));
#53608=CARTESIAN_POINT('Ctrl Pts',(132.288803122879,3.95062462725389,332.067336293825));
#53609=CARTESIAN_POINT('Ctrl Pts',(132.281051149356,3.86730775941755,331.958301365523));
#53610=CARTESIAN_POINT('Ctrl Pts',(132.273299175833,3.77953192755591,331.852886803579));
#53611=CARTESIAN_POINT('Ctrl Pts',(132.265550485275,3.69179326881099,331.747516884765));
#53612=CARTESIAN_POINT('Ctrl Pts',(132.257801794718,3.59959965147738,331.645764582577));
#53613=CARTESIAN_POINT('Ctrl Pts',(132.25005310416,3.50328759068137,331.548020985076));
#53614=CARTESIAN_POINT('Ctrl Pts',(132.242306025782,3.40699556841402,331.450297723946));
#53615=CARTESIAN_POINT('Ctrl Pts',(132.234558947404,3.3065870812436,331.356581786774));
#53616=CARTESIAN_POINT('Ctrl Pts',(132.226811869027,3.2024365677531,331.267228497213));
#53617=CARTESIAN_POINT('Ctrl Pts',(132.219064725721,3.09828518138123,331.177874458786));
#53618=CARTESIAN_POINT('Ctrl Pts',(132.211317582415,2.99039200279513,331.09288339541));
#53619=CARTESIAN_POINT('Ctrl Pts',(132.203570439109,2.8791654025531,331.012571048001));
#53620=CARTESIAN_POINT('Ctrl Pts',(132.195821554081,2.76791379620974,330.932240644671));
#53621=CARTESIAN_POINT('Ctrl Pts',(132.188072669053,2.65332759377652,330.856591279197));
#53622=CARTESIAN_POINT('Ctrl Pts',(132.180323784025,2.53584471459587,330.785895748091));
#53623=CARTESIAN_POINT('Ctrl Pts',(132.17256667425,2.41823713787328,330.715125180018));
#53624=CARTESIAN_POINT('Ctrl Pts',(132.164809564475,2.29772707811779,330.649319151615));
#53625=CARTESIAN_POINT('Ctrl Pts',(132.157052454701,2.17477814896891,330.588705058005));
#53626=CARTESIAN_POINT('Ctrl Pts',(132.149291199775,2.05176351984357,330.528058574163));
#53627=CARTESIAN_POINT('Ctrl Pts',(132.141529944848,1.92630778180462,330.472609711296));
#53628=CARTESIAN_POINT('Ctrl Pts',(132.133768689922,1.79889423665548,330.422537538349));
#53629=CARTESIAN_POINT('Ctrl Pts',(132.125995019518,1.67127687135808,330.372385266243));
#53630=CARTESIAN_POINT('Ctrl Pts',(132.118221349113,1.54169581023032,330.327626998984));
#53631=CARTESIAN_POINT('Ctrl Pts',(132.110447678708,1.41065006155037,330.288392050865));
#53632=CARTESIAN_POINT('Ctrl Pts',(132.103035874531,1.28570452399904,330.250983499021));
#53633=CARTESIAN_POINT('Ctrl Pts',(132.095624070354,1.15942787132853,330.218595689027));
#53634=CARTESIAN_POINT('Ctrl Pts',(132.088212266177,1.03225910621512,330.191297035568));
#53635=CARTESIAN_POINT('Ctrl Pts',(132.080437187398,0.898857421107762,330.162660393784));
#53636=CARTESIAN_POINT('Ctrl Pts',(132.07266210862,0.764052388230484,330.139533894822));
#53637=CARTESIAN_POINT('Ctrl Pts',(132.064887029842,0.628338922813376,330.122052351595));
#53638=CARTESIAN_POINT('Ctrl Pts',(132.057121518793,0.492792461454992,330.104592320521));
#53639=CARTESIAN_POINT('Ctrl Pts',(132.049356007744,0.356340175790856,330.092763473144));
#53640=CARTESIAN_POINT('Ctrl Pts',(132.041590496695,0.219489106663411,330.086650063902));
#53641=CARTESIAN_POINT('Ctrl Pts',(132.033832685172,0.0827737257694367,
330.080542716123));
#53642=CARTESIAN_POINT('Ctrl Pts',(132.02607487365,-0.0543392637600575,
330.080139546411));
#53643=CARTESIAN_POINT('Ctrl Pts',(132.018317062128,-0.19133608088388,330.085473210303));
#53644=CARTESIAN_POINT('Ctrl Pts',(132.010565088605,-0.328229803559003,
330.090802860443));
#53645=CARTESIAN_POINT('Ctrl Pts',(132.002813115082,-0.465007138834769,
330.101860735967));
#53646=CARTESIAN_POINT('Ctrl Pts',(131.995061141559,-0.601153032092159,
330.118627437441));
#53647=CARTESIAN_POINT('Ctrl Pts',(131.987312451001,-0.737241267482229,
330.135387038206));
#53648=CARTESIAN_POINT('Ctrl Pts',(131.979563760443,-0.872698205589537,
330.157850608628));
#53649=CARTESIAN_POINT('Ctrl Pts',(131.971815069886,-1.00701286447879,330.185946806144));
#53650=CARTESIAN_POINT('Ctrl Pts',(131.964067991508,-1.14129957808145,330.214037158012));
#53651=CARTESIAN_POINT('Ctrl Pts',(131.95632091313,-1.27444410283695,330.247757725972));
#53652=CARTESIAN_POINT('Ctrl Pts',(131.948573834752,-1.40594500930237,330.286985922648));
#53653=CARTESIAN_POINT('Ctrl Pts',(131.940826691446,-1.53744701787186,330.326214448094));
#53654=CARTESIAN_POINT('Ctrl Pts',(131.933079548141,-1.66730500611248,330.370950582588));
#53655=CARTESIAN_POINT('Ctrl Pts',(131.925332404835,-1.79503246800941,330.421021784143));
#53656=CARTESIAN_POINT('Ctrl Pts',(131.917583519807,-1.92278864575208,330.471104242767));
#53657=CARTESIAN_POINT('Ctrl Pts',(131.909834634779,-2.04841298017952,330.526524012566));
#53658=CARTESIAN_POINT('Ctrl Pts',(131.90208574975,-2.17143908760112,330.587060463666));
#53659=CARTESIAN_POINT('Ctrl Pts',(131.894328639976,-2.29459577620373,330.647661168781));
#53660=CARTESIAN_POINT('Ctrl Pts',(131.886571530201,-2.41514837759722,330.713389231081));
#53661=CARTESIAN_POINT('Ctrl Pts',(131.878814420426,-2.53265478242858,330.783977844515));
#53662=CARTESIAN_POINT('Ctrl Pts',(131.8710531655,-2.6502239789256,330.854604178247));
#53663=CARTESIAN_POINT('Ctrl Pts',(131.863291910574,-2.76474340916123,330.930096023493));
#53664=CARTESIAN_POINT('Ctrl Pts',(131.855530655648,-2.87580094790362,331.010143865935));
#53665=CARTESIAN_POINT('Ctrl Pts',(131.847756985243,-2.98703614251424,331.090319758837));
#53666=CARTESIAN_POINT('Ctrl Pts',(131.839983314838,-3.09479807186334,331.175065970988));
#53667=CARTESIAN_POINT('Ctrl Pts',(131.832209644434,-3.19870795079148,331.264032855064));
#53668=CARTESIAN_POINT('Ctrl Pts',(131.824797840257,-3.29778079985462,331.34885830928));
#53669=CARTESIAN_POINT('Ctrl Pts',(131.81738603608,-3.39335194275258,331.437520138104));
#53670=CARTESIAN_POINT('Ctrl Pts',(131.809974231903,-3.48512627858102,331.529686197929));
#53671=CARTESIAN_POINT('Ctrl Pts',(131.802305934558,-3.58007656045564,331.625041759816));
#53672=CARTESIAN_POINT('Ctrl Pts',(131.794637637212,-3.67128062595262,331.724468265431));
#53673=CARTESIAN_POINT('Ctrl Pts',(131.786969339867,-3.75836182038182,331.827635032094));
#53674=CARTESIAN_POINT('Ctrl Pts',(131.779310663728,-3.84533375638371,331.930672358197));
#53675=CARTESIAN_POINT('Ctrl Pts',(131.771651987588,-3.9281928520073,332.037440307722));
#53676=CARTESIAN_POINT('Ctrl Pts',(131.763993311449,-4.0065979590162,332.147570183632));
#53677=CARTESIAN_POINT('Ctrl Pts',(131.756343468794,-4.08491263390531,332.257573036207));
#53678=CARTESIAN_POINT('Ctrl Pts',(131.74869362614,-4.15878331438801,332.370929770508));
#53679=CARTESIAN_POINT('Ctrl Pts',(131.741043783485,-4.22790843468976,332.487237908122));
#53680=CARTESIAN_POINT('Ctrl Pts',(131.73339888633,-4.29698886672092,332.603470854409));
#53681=CARTESIAN_POINT('Ctrl Pts',(131.725753989175,-4.36132963354344,332.722651065717));
#53682=CARTESIAN_POINT('Ctrl Pts',(131.71810909202,-4.42067198370221,332.84434643901));
#53683=CARTESIAN_POINT('Ctrl Pts',(131.710467374888,-4.47998964941481,332.96599119107));
#53684=CARTESIAN_POINT('Ctrl Pts',(131.702825657756,-4.53431285765914,333.090148663068));
#53685=CARTESIAN_POINT('Ctrl Pts',(131.695183940624,-4.58342867096348,333.216361953565));
#53686=CARTESIAN_POINT('Ctrl Pts',(131.68754364097,-4.63253537367045,333.342551832489));
#53687=CARTESIAN_POINT('Ctrl Pts',(131.679903341317,-4.6764364583927,333.470796395842));
#53688=CARTESIAN_POINT('Ctrl Pts',(131.672263041663,-4.71496724219373,333.600619077042));
#53689=CARTESIAN_POINT('Ctrl Pts',(131.664619815753,-4.75351278339635,333.730491480703));
#53690=CARTESIAN_POINT('Ctrl Pts',(131.656976589842,-4.78668379738941,333.861942824209));
#53691=CARTESIAN_POINT('Ctrl Pts',(131.649333363932,-4.81436559811462,333.994481750444));
#53692=CARTESIAN_POINT('Ctrl Pts',(131.641688538834,-4.84205319068665,334.12704840772));
#53693=CARTESIAN_POINT('Ctrl Pts',(131.634043713736,-4.86424921182576,334.260702704538));
#53694=CARTESIAN_POINT('Ctrl Pts',(131.626398888638,-4.88089039629261,334.39494462908));
#53695=CARTESIAN_POINT('Ctrl Pts',(131.618747285445,-4.89754633525291,334.529305575896));
#53696=CARTESIAN_POINT('Ctrl Pts',(131.611095682253,-4.90863756668902,334.66425478993));
#53697=CARTESIAN_POINT('Ctrl Pts',(131.60344407906,-4.91415282542032,334.799288587984));
#53698=CARTESIAN_POINT('Ctrl Pts',(131.599568511552,-4.91694632594542,334.867683744793));
#53699=CARTESIAN_POINT('Ctrl Pts',(131.595692944044,-4.91831016231917,334.936100601925));
#53700=CARTESIAN_POINT('Ctrl Pts',(131.591817376536,-4.91824796507461,335.004473984742));
#53701=CARTESIAN_POINT('',(129.841817376473,-4.91824953106053,334.997852274953));
#53702=CARTESIAN_POINT('Ctrl Pts',(131.591817376508,-4.91824796507415,335.004473985242));
#53703=CARTESIAN_POINT('Ctrl Pts',(131.581074090443,-4.91807555087569,335.194008759026));
#53704=CARTESIAN_POINT('Ctrl Pts',(131.570330804377,-4.90694353044546,335.383064788424));
#53705=CARTESIAN_POINT('Ctrl Pts',(131.559587518311,-4.88503791690134,335.570602850445));
#53706=CARTESIAN_POINT('Ctrl Pts',(131.550303744751,-4.86610825658985,335.732663219235));
#53707=CARTESIAN_POINT('Ctrl Pts',(131.54101997119,-4.83913421272028,335.893590931491));
#53708=CARTESIAN_POINT('Ctrl Pts',(131.531736197629,-4.80426271790346,336.052731114703));
#53709=CARTESIAN_POINT('Ctrl Pts',(131.523961118851,-4.77505814741838,336.18600961974));
#53710=CARTESIAN_POINT('Ctrl Pts',(131.516186040072,-4.74025716358077,336.318282532187));
#53711=CARTESIAN_POINT('Ctrl Pts',(131.508410961294,-4.69994210963483,336.449043556482));
#53712=CARTESIAN_POINT('Ctrl Pts',(131.500645450245,-4.65967666592935,336.579643671011));
#53713=CARTESIAN_POINT('Ctrl Pts',(131.492879939196,-4.61391076720518,336.708735229245));
#53714=CARTESIAN_POINT('Ctrl Pts',(131.485114428147,-4.56277779568918,336.835821845841));
#53715=CARTESIAN_POINT('Ctrl Pts',(131.477356616625,-4.51169552266329,336.962782455686));
#53716=CARTESIAN_POINT('Ctrl Pts',(131.469598805102,-4.45525691182909,337.087741719651));
#53717=CARTESIAN_POINT('Ctrl Pts',(131.46184099358,-4.39364510016533,337.210218495148));
#53718=CARTESIAN_POINT('Ctrl Pts',(131.454089020057,-4.33207965334384,337.332603102987));
#53719=CARTESIAN_POINT('Ctrl Pts',(131.446337046534,-4.26534892946257,337.452508593045));
#53720=CARTESIAN_POINT('Ctrl Pts',(131.438585073011,-4.19368397053202,337.569474229838));
#53721=CARTESIAN_POINT('Ctrl Pts',(131.430836382454,-4.12204936175401,337.686390331615));
#53722=CARTESIAN_POINT('Ctrl Pts',(131.423087691896,-4.04548487787832,337.800368723805));
#53723=CARTESIAN_POINT('Ctrl Pts',(131.415339001338,-3.96426714921201,337.910973897543));
#53724=CARTESIAN_POINT('Ctrl Pts',(131.40759192296,-3.88306631857247,338.021556058951));
#53725=CARTESIAN_POINT('Ctrl Pts',(131.399844844583,-3.79721440005633,338.12876608303));
#53726=CARTESIAN_POINT('Ctrl Pts',(131.392097766205,-3.70703070643482,338.232198385627));
#53727=CARTESIAN_POINT('Ctrl Pts',(131.384350622899,-3.61684625698725,338.335631555086));
#53728=CARTESIAN_POINT('Ctrl Pts',(131.376603479593,-3.52233021689897,338.435286645299));
#53729=CARTESIAN_POINT('Ctrl Pts',(131.368856336287,-3.4238411819727,338.53079235061));
#53730=CARTESIAN_POINT('Ctrl Pts',(131.361107451259,-3.32533000462047,338.626319527632));
#53731=CARTESIAN_POINT('Ctrl Pts',(131.353358566231,-3.22284433558728,338.717695191391));
#53732=CARTESIAN_POINT('Ctrl Pts',(131.345609681203,-3.11677820083286,338.804586273081));
#53733=CARTESIAN_POINT('Ctrl Pts',(131.337852571428,-3.010599486387,338.891569581862));
#53734=CARTESIAN_POINT('Ctrl Pts',(131.330095461654,-2.90083301752187,338.974058551969));
#53735=CARTESIAN_POINT('Ctrl Pts',(131.322338351879,-2.78790479026287,339.051761338348));
#53736=CARTESIAN_POINT('Ctrl Pts',(131.314577096953,-2.67491621777008,339.129505646611));
#53737=CARTESIAN_POINT('Ctrl Pts',(131.306815842027,-2.55876285115244,339.202458467142));
#53738=CARTESIAN_POINT('Ctrl Pts',(131.2990545871,-2.4398971346612,339.270372938605));
#53739=CARTESIAN_POINT('Ctrl Pts',(131.291280916696,-2.3208412717617,339.33839605109));
#53740=CARTESIAN_POINT('Ctrl Pts',(131.283507246291,-2.19906473601633,339.401364529178));
#53741=CARTESIAN_POINT('Ctrl Pts',(131.275733575886,-2.07504268568888,339.459078482721));
#53742=CARTESIAN_POINT('Ctrl Pts',(131.268321771709,-1.95679389164187,339.514105837842));
#53743=CARTESIAN_POINT('Ctrl Pts',(131.260909967532,-1.83650420126968,339.56435674466));
#53744=CARTESIAN_POINT('Ctrl Pts',(131.253498163355,-1.71459817180724,339.609700225799));
#53745=CARTESIAN_POINT('Ctrl Pts',(131.245723084577,-1.58671716470171,339.657266126021));
#53746=CARTESIAN_POINT('Ctrl Pts',(131.237948005798,-1.4566532414712,339.699581699009));
#53747=CARTESIAN_POINT('Ctrl Pts',(131.23017292702,-1.32487671751047,339.736442203374));
#53748=CARTESIAN_POINT('Ctrl Pts',(131.222407415971,-1.19326235295174,339.773257348541));
#53749=CARTESIAN_POINT('Ctrl Pts',(131.214641904922,-1.05993995373909,339.804630677363));
#53750=CARTESIAN_POINT('Ctrl Pts',(131.206876393873,-0.925399121672873,
339.83040573121));
#53751=CARTESIAN_POINT('Ctrl Pts',(131.19911858235,-0.790991687233353,339.856155229016));
#53752=CARTESIAN_POINT('Ctrl Pts',(131.191360770828,-0.655368605507206,
339.876317424993));
#53753=CARTESIAN_POINT('Ctrl Pts',(131.183602959306,-0.51903358548839,339.890785949071));
#53754=CARTESIAN_POINT('Ctrl Pts',(131.175850985783,-0.38280116189571,339.905243585127));
#53755=CARTESIAN_POINT('Ctrl Pts',(131.16809901226,-0.245858253533314,339.914016036624));
#53756=CARTESIAN_POINT('Ctrl Pts',(131.160347038737,-0.108717332789754,
339.91704826131));
#53757=CARTESIAN_POINT('Ctrl Pts',(131.152598348179,0.028365508692543,339.920079201847));
#53758=CARTESIAN_POINT('Ctrl Pts',(131.144849657622,0.165645805802129,339.917374742017));
#53759=CARTESIAN_POINT('Ctrl Pts',(131.137100967064,0.302607629310269,339.908931827311));
#53760=CARTESIAN_POINT('Ctrl Pts',(131.129353888686,0.439540956767055,339.900490669223));
#53761=CARTESIAN_POINT('Ctrl Pts',(131.121606810308,0.576155552531599,339.886313455111));
#53762=CARTESIAN_POINT('Ctrl Pts',(131.113859731931,0.711937553774379,339.86644921704));
#53763=CARTESIAN_POINT('Ctrl Pts',(131.106112588625,0.847720693001064,339.846584812486));
#53764=CARTESIAN_POINT('Ctrl Pts',(131.098365445319,0.98267083703049,339.821033345487));
#53765=CARTESIAN_POINT('Ctrl Pts',(131.090618302013,1.11628169025015,339.789895432106));
#53766=CARTESIAN_POINT('Ctrl Pts',(131.082869416985,1.24992258202608,339.758750518261));
#53767=CARTESIAN_POINT('Ctrl Pts',(131.075120531957,1.38222320323586,339.72201674753));
#53768=CARTESIAN_POINT('Ctrl Pts',(131.067371646929,1.51269023915775,339.679845222105));
#53769=CARTESIAN_POINT('Ctrl Pts',(131.059614537154,1.64329575413968,339.637628935386));
#53770=CARTESIAN_POINT('Ctrl Pts',(131.051857427379,1.77206342362917,339.589963484894));
#53771=CARTESIAN_POINT('Ctrl Pts',(131.044100317605,1.89851729800148,339.537049165668));
#53772=CARTESIAN_POINT('Ctrl Pts',(131.036339062678,2.02503874528109,339.484106570722));
#53773=CARTESIAN_POINT('Ctrl Pts',(131.028577807752,2.14924358000155,339.425909683931));
#53774=CARTESIAN_POINT('Ctrl Pts',(131.020816552826,2.27067936765368,339.362705384485));
#53775=CARTESIAN_POINT('Ctrl Pts',(131.013042882421,2.39230941299019,339.299399978758));
#53776=CARTESIAN_POINT('Ctrl Pts',(131.005269212017,2.51116122061661,339.231071348485));
#53777=CARTESIAN_POINT('Ctrl Pts',(130.997495541612,2.62680956324,339.158010892358));
#53778=CARTESIAN_POINT('Ctrl Pts',(130.990083737435,2.73707444768979,339.088351418042));
#53779=CARTESIAN_POINT('Ctrl Pts',(130.982671933258,2.84442716096901,339.014390900217));
#53780=CARTESIAN_POINT('Ctrl Pts',(130.975260129081,2.9485278091276,338.936415478745));
#53781=CARTESIAN_POINT('Ctrl Pts',(130.967485050303,3.05773074015337,338.854618249589));
#53782=CARTESIAN_POINT('Ctrl Pts',(130.959709971524,3.16369986016846,338.768144106363));
#53783=CARTESIAN_POINT('Ctrl Pts',(130.951934892746,3.2660084831235,338.677277750003));
#53784=CARTESIAN_POINT('Ctrl Pts',(130.944169381697,3.36819120880474,338.586523210479));
#53785=CARTESIAN_POINT('Ctrl Pts',(130.936403870648,3.46672211058377,338.491387469099));
#53786=CARTESIAN_POINT('Ctrl Pts',(130.928638359599,3.56120466743245,338.392197573721));
#53787=CARTESIAN_POINT('Ctrl Pts',(130.920880548077,3.65559354455092,338.293106025412));
#53788=CARTESIAN_POINT('Ctrl Pts',(130.913122736554,3.74594179686235,338.189968603747));
#53789=CARTESIAN_POINT('Ctrl Pts',(130.905364925032,3.83188738966656,338.083151325416));
#53790=CARTESIAN_POINT('Ctrl Pts',(130.897612951509,3.91776830568666,337.976414430474));
#53791=CARTESIAN_POINT('Ctrl Pts',(130.889860977986,3.99925291279998,337.866003494152));
#53792=CARTESIAN_POINT('Ctrl Pts',(130.882109004463,4.07601759658679,337.752319678892));
#53793=CARTESIAN_POINT('Ctrl Pts',(130.874360313905,4.15274977048444,337.638684008795));
#53794=CARTESIAN_POINT('Ctrl Pts',(130.866611623348,4.22476577842427,337.521778539813));
#53795=CARTESIAN_POINT('Ctrl Pts',(130.85886293279,4.29178385289398,337.402035474871));
#53796=CARTESIAN_POINT('Ctrl Pts',(130.851115854412,4.35878798369353,337.282317323473));
#53797=CARTESIAN_POINT('Ctrl Pts',(130.843368776035,4.42079605860149,337.159763091306));
#53798=CARTESIAN_POINT('Ctrl Pts',(130.835621697657,4.47757122906411,337.034831430649));
#53799=CARTESIAN_POINT('Ctrl Pts',(130.827874554351,4.53434687535731,336.909898722944));
#53800=CARTESIAN_POINT('Ctrl Pts',(130.820127411045,4.58588936801282,336.782588902859));
#53801=CARTESIAN_POINT('Ctrl Pts',(130.812380267739,4.63200933161903,336.6533821743));
#53802=CARTESIAN_POINT('Ctrl Pts',(130.804631382711,4.6781396639722,336.524146397326));
#53803=CARTESIAN_POINT('Ctrl Pts',(130.796882497683,4.71884491002831,336.393013231315));
#53804=CARTESIAN_POINT('Ctrl Pts',(130.789133612655,4.75398517394242,336.260479285207));
#53805=CARTESIAN_POINT('Ctrl Pts',(130.78137650288,4.78916273609574,336.127804666199));
#53806=CARTESIAN_POINT('Ctrl Pts',(130.773619393106,4.81876341652676,335.993726675483));
#53807=CARTESIAN_POINT('Ctrl Pts',(130.765862283331,4.84269808395704,335.858753940392));
#53808=CARTESIAN_POINT('Ctrl Pts',(130.758101028405,4.8666455413083,335.723709080187));
#53809=CARTESIAN_POINT('Ctrl Pts',(130.750339773478,4.8849209005688,335.587768910098));
#53810=CARTESIAN_POINT('Ctrl Pts',(130.742578518552,4.89748692944257,335.45144749245));
#53811=CARTESIAN_POINT('Ctrl Pts',(130.734804848148,4.91007305986728,335.314908004961));
#53812=CARTESIAN_POINT('Ctrl Pts',(130.727031177743,4.91693158976578,335.177986441799));
#53813=CARTESIAN_POINT('Ctrl Pts',(130.719257507338,4.91807744762636,335.04119807822));
#53814=CARTESIAN_POINT('Ctrl Pts',(130.711845703161,4.91916996552786,334.910777245874));
#53815=CARTESIAN_POINT('Ctrl Pts',(130.704433898984,4.91506970126257,334.780477778956));
#53816=CARTESIAN_POINT('Ctrl Pts',(130.697022094807,4.90583333982647,334.650740348241));
#53817=CARTESIAN_POINT('Ctrl Pts',(130.689247016028,4.89614427680274,334.514644099578));
#53818=CARTESIAN_POINT('Ctrl Pts',(130.68147193725,4.8807722962662,334.378736285021));
#53819=CARTESIAN_POINT('Ctrl Pts',(130.673696858472,4.85972590500248,334.243529781982));
#53820=CARTESIAN_POINT('Ctrl Pts',(130.665931347423,4.83870541266309,334.108489659153));
#53821=CARTESIAN_POINT('Ctrl Pts',(130.658165836374,4.8120244627596,333.974149513234));
#53822=CARTESIAN_POINT('Ctrl Pts',(130.650400325325,4.77974349653092,333.841019771579));
#53823=CARTESIAN_POINT('Ctrl Pts',(130.642642513802,4.74749453697426,333.70802202845));
#53824=CARTESIAN_POINT('Ctrl Pts',(130.63488470228,4.70965670226278,333.576232678699));
#53825=CARTESIAN_POINT('Ctrl Pts',(130.627126890758,4.66634186589082,333.446154237662));
#53826=CARTESIAN_POINT('Ctrl Pts',(130.619374917235,4.62305962530683,333.316173684777));
#53827=CARTESIAN_POINT('Ctrl Pts',(130.611622943712,4.57430870993389,333.187901847236));
#53828=CARTESIAN_POINT('Ctrl Pts',(130.603870970189,4.52025133949755,333.061827951324));
#53829=CARTESIAN_POINT('Ctrl Pts',(130.596122279631,4.46621686238968,332.935807447781));
#53830=CARTESIAN_POINT('Ctrl Pts',(130.588373589074,4.40688055362788,332.81198339301));
#53831=CARTESIAN_POINT('Ctrl Pts',(130.580624898516,4.34245338130343,332.690826621125));
#53832=CARTESIAN_POINT('Ctrl Pts',(130.572877820138,4.27803961359029,332.569695056918));
#53833=CARTESIAN_POINT('Ctrl Pts',(130.56513074176,4.20853727253625,332.451230016657));
#53834=CARTESIAN_POINT('Ctrl Pts',(130.557383663382,4.13420387628524,332.335878874411));
#53835=CARTESIAN_POINT('Ctrl Pts',(130.549636520077,4.0598698570488,332.220526765412));
#53836=CARTESIAN_POINT('Ctrl Pts',(130.541889376771,3.98070491358631,332.108288935043));
#53837=CARTESIAN_POINT('Ctrl Pts',(130.534142233465,3.89701037770713,331.999584499016));
#53838=CARTESIAN_POINT('Ctrl Pts',(130.526393348437,3.81329702551945,331.890855623925));
#53839=CARTESIAN_POINT('Ctrl Pts',(130.518644463409,3.72505229292445,331.78566203356));
#53840=CARTESIAN_POINT('Ctrl Pts',(130.510895578381,3.63261808330605,331.684390112915));
#53841=CARTESIAN_POINT('Ctrl Pts',(130.503138468606,3.54008576306248,331.583010701206));
#53842=CARTESIAN_POINT('Ctrl Pts',(130.495381358831,3.44335534690867,331.485561563359));
#53843=CARTESIAN_POINT('Ctrl Pts',(130.487624249057,3.34280631637109,331.392392899202));
#53844=CARTESIAN_POINT('Ctrl Pts',(130.47986299413,3.24220355564657,331.299174448689));
#53845=CARTESIAN_POINT('Ctrl Pts',(130.472101739204,3.13777841199752,331.210241282919));
#53846=CARTESIAN_POINT('Ctrl Pts',(130.464340484278,3.02994302286966,331.125902899944));
#53847=CARTESIAN_POINT('Ctrl Pts',(130.456566813873,2.92193513226267,331.041429603042));
#53848=CARTESIAN_POINT('Ctrl Pts',(130.448793143469,2.810506412777,330.961566004546));
#53849=CARTESIAN_POINT('Ctrl Pts',(130.441019473064,2.69609824902881,330.886578395778));
#53850=CARTESIAN_POINT('Ctrl Pts',(130.433607668887,2.58701581282919,330.815081478239));
#53851=CARTESIAN_POINT('Ctrl Pts',(130.42619586471,2.47522532301588,330.748016959806));
#53852=CARTESIAN_POINT('Ctrl Pts',(130.418784060533,2.36112802454671,330.685575645095));
#53853=CARTESIAN_POINT('Ctrl Pts',(130.411008981755,2.24143847760014,330.620073895546));
#53854=CARTESIAN_POINT('Ctrl Pts',(130.403233902976,2.11883203616041,330.55945300508));
#53855=CARTESIAN_POINT('Ctrl Pts',(130.395458824198,1.99374459329656,330.503983367557));
#53856=CARTESIAN_POINT('Ctrl Pts',(130.387693313149,1.86881107849457,330.448581988955));
#53857=CARTESIAN_POINT('Ctrl Pts',(130.3799278021,1.74140299082494,330.398319407549));
#53858=CARTESIAN_POINT('Ctrl Pts',(130.372162291051,1.61198226776083,330.353421018542));
#53859=CARTESIAN_POINT('Ctrl Pts',(130.364404479528,1.48268986572056,330.308567146419));
#53860=CARTESIAN_POINT('Ctrl Pts',(130.356646668006,1.35138916641562,330.269067009641));
#53861=CARTESIAN_POINT('Ctrl Pts',(130.348888856484,1.21856328688035,330.235098471283));
#53862=CARTESIAN_POINT('Ctrl Pts',(130.341136882961,1.08583736303154,330.201155495328));
#53863=CARTESIAN_POINT('Ctrl Pts',(130.333384909438,0.951588920647927,330.17273592859));
#53864=CARTESIAN_POINT('Ctrl Pts',(130.325632935915,0.816317146952556,330.149968105456));
#53865=CARTESIAN_POINT('Ctrl Pts',(130.317884245357,0.681102660933657,330.12720992451));
#53866=CARTESIAN_POINT('Ctrl Pts',(130.3101355548,0.544866090218616,330.110098791372));
#53867=CARTESIAN_POINT('Ctrl Pts',(130.302386864242,0.40811753619882,330.098712093832));
#53868=CARTESIAN_POINT('Ctrl Pts',(130.294639785864,0.271397433857881,330.087327765389));
#53869=CARTESIAN_POINT('Ctrl Pts',(130.286892707487,0.134165949374462,330.081665535942));
#53870=CARTESIAN_POINT('Ctrl Pts',(130.279145629109,-0.00306135300955948,
330.081750952766));
#53871=CARTESIAN_POINT('Ctrl Pts',(130.271398485803,-0.140289805490502,
330.081836370306));
#53872=CARTESIAN_POINT('Ctrl Pts',(130.263651342497,-0.277513684927922,
330.087669529956));
#53873=CARTESIAN_POINT('Ctrl Pts',(130.255904199191,-0.41421748004531,330.099223842928));
#53874=CARTESIAN_POINT('Ctrl Pts',(130.248155314163,-0.550952009078004,
330.110780753555));
#53875=CARTESIAN_POINT('Ctrl Pts',(130.240406429135,-0.687165831711539,
330.12806134406));
#53876=CARTESIAN_POINT('Ctrl Pts',(130.232657544107,-0.822349005022078,
330.150987195682));
#53877=CARTESIAN_POINT('Ctrl Pts',(130.224900434332,-0.957675663149658,
330.17393738104));
#53878=CARTESIAN_POINT('Ctrl Pts',(130.217143324558,-1.09196910072239,330.202544731517));
#53879=CARTESIAN_POINT('Ctrl Pts',(130.209386214783,-1.22472946800457,330.236679646224));
#53880=CARTESIAN_POINT('Ctrl Pts',(130.201624959857,-1.35756077818208,330.270832801537));
#53881=CARTESIAN_POINT('Ctrl Pts',(130.193863704931,-1.48885701172631,330.310519293661));
#53882=CARTESIAN_POINT('Ctrl Pts',(130.186102450004,-1.61813487390069,330.355560034583));
#53883=CARTESIAN_POINT('Ctrl Pts',(130.1783287796,-1.74761953852298,330.400672826011));
#53884=CARTESIAN_POINT('Ctrl Pts',(130.170555109195,-1.87507901620582,330.451156837735));
#53885=CARTESIAN_POINT('Ctrl Pts',(130.16278143879,-2.00005051835259,330.506785005529));
#53886=CARTESIAN_POINT('Ctrl Pts',(130.155369634613,-2.11920456700869,330.55982366873));
#53887=CARTESIAN_POINT('Ctrl Pts',(130.147957830436,-2.23609679989502,330.617538217474));
#53888=CARTESIAN_POINT('Ctrl Pts',(130.140546026259,-2.35034962866728,330.679694491645));
#53889=CARTESIAN_POINT('Ctrl Pts',(130.132770947481,-2.47020232891869,330.744897229967));
#53890=CARTESIAN_POINT('Ctrl Pts',(130.124995868702,-2.58752910962054,330.81519416001));
#53891=CARTESIAN_POINT('Ctrl Pts',(130.117220789924,-2.70186670405607,330.890365055627));
#53892=CARTESIAN_POINT('Ctrl Pts',(130.109455278875,-2.81606359880259,330.965443448671));
#53893=CARTESIAN_POINT('Ctrl Pts',(130.101689767826,-2.9272783027243,331.04538366086));
#53894=CARTESIAN_POINT('Ctrl Pts',(130.093924256777,-3.03507129531473,331.129919213394));
#53895=CARTESIAN_POINT('Ctrl Pts',(130.086166445255,-3.142757410839,331.214370948682));
#53896=CARTESIAN_POINT('Ctrl Pts',(130.078408633732,-3.24702826098043,331.303408717377));
#53897=CARTESIAN_POINT('Ctrl Pts',(130.07065082221,-3.34747283453631,331.396722507974));
#53898=CARTESIAN_POINT('Ctrl Pts',(130.062898848687,-3.44784182036548,331.489966076985));
#53899=CARTESIAN_POINT('Ctrl Pts',(130.055146875164,-3.54438997568825,331.587478997974));
#53900=CARTESIAN_POINT('Ctrl Pts',(130.047394901641,-3.63673924253068,331.688910942856));
#53901=CARTESIAN_POINT('Ctrl Pts',(130.039646211084,-3.72904939940371,331.79029993125));
#53902=CARTESIAN_POINT('Ctrl Pts',(130.031897520526,-3.81716394197539,331.895604354067));
#53903=CARTESIAN_POINT('Ctrl Pts',(130.024148829968,-3.90074174807203,332.004437135137));
#53904=CARTESIAN_POINT('Ctrl Pts',(130.016401751591,-3.98430216510805,332.113247272638));
#53905=CARTESIAN_POINT('Ctrl Pts',(130.008654673213,-4.06332748524398,332.225583998392));
#53906=CARTESIAN_POINT('Ctrl Pts',(130.000907594835,-4.13751722383503,332.341027588528));
#53907=CARTESIAN_POINT('Ctrl Pts',(129.993160451529,-4.21170758420752,332.456472146192));
#53908=CARTESIAN_POINT('Ctrl Pts',(129.985413308223,-4.28106207088147,332.575023291347));
#53909=CARTESIAN_POINT('Ctrl Pts',(129.977666164917,-4.34532407020271,332.696233130845));
#53910=CARTESIAN_POINT('Ctrl Pts',(129.969917279889,-4.40960051698553,332.817470220887));
#53911=CARTESIAN_POINT('Ctrl Pts',(129.962168394861,-4.46878201513965,332.941366849416));
#53912=CARTESIAN_POINT('Ctrl Pts',(129.954419509833,-4.52265854929574,333.067451757657));
#53913=CARTESIAN_POINT('Ctrl Pts',(129.946662400058,-4.57659226856202,333.193670493723));
#53914=CARTESIAN_POINT('Ctrl Pts',(129.938905290284,-4.62520962206125,333.322081789236));
#53915=CARTESIAN_POINT('Ctrl Pts',(129.931148180509,-4.66834909657316,333.45219517541));
#53916=CARTESIAN_POINT('Ctrl Pts',(129.923386925583,-4.71151162344086,333.582378090017));
#53917=CARTESIAN_POINT('Ctrl Pts',(129.915625670657,-4.74919033128616,333.714264531986));
#53918=CARTESIAN_POINT('Ctrl Pts',(129.90786441573,-4.78127428052794,333.84735117366));
#53919=CARTESIAN_POINT('Ctrl Pts',(129.900090745326,-4.81340955363239,333.980650710589));
#53920=CARTESIAN_POINT('Ctrl Pts',(129.892317074921,-4.83993210814188,334.115153900117));
#53921=CARTESIAN_POINT('Ctrl Pts',(129.884543404516,-4.8607824457437,334.250348695959));
#53922=CARTESIAN_POINT('Ctrl Pts',(129.877131600339,-4.88066219511398,334.37925014153));
#53923=CARTESIAN_POINT('Ctrl Pts',(129.869719796162,-4.89538589427849,334.508779967937));
#53924=CARTESIAN_POINT('Ctrl Pts',(129.862307991985,-4.90494611875688,334.638493935608));
#53925=CARTESIAN_POINT('Ctrl Pts',(129.855477786826,-4.91375615919946,334.758029340216));
#53926=CARTESIAN_POINT('Ctrl Pts',(129.848647581667,-4.91819714564155,334.877890695419));
#53927=CARTESIAN_POINT('Ctrl Pts',(129.841817376508,-4.91824953106026,334.997852274342));
#53928=CARTESIAN_POINT('',(128.091817376563,-4.91824887636649,334.996675451945));
#53929=CARTESIAN_POINT('Ctrl Pts',(129.841817376473,-4.91824953106053,334.997852274953));
#53930=CARTESIAN_POINT('Ctrl Pts',(129.834124842131,-4.91830853024261,335.1329592804));
#53931=CARTESIAN_POINT('Ctrl Pts',(129.826432307789,-4.91279613065993,335.268293179147));
#53932=CARTESIAN_POINT('Ctrl Pts',(129.818739773447,-4.90168251187349,335.403350486914));
#53933=CARTESIAN_POINT('Ctrl Pts',(129.811056230747,-4.89058188356311,335.538249929025));
#53934=CARTESIAN_POINT('Ctrl Pts',(129.803372688047,-4.87389309065989,335.672873028552));
#53935=CARTESIAN_POINT('Ctrl Pts',(129.795689145347,-4.85163830171469,335.806714851627));
#53936=CARTESIAN_POINT('Ctrl Pts',(129.788012653009,-4.82940393360061,335.940433862426));
#53937=CARTESIAN_POINT('Ctrl Pts',(129.780336160671,-4.80161379497764,336.073372630984));
#53938=CARTESIAN_POINT('Ctrl Pts',(129.772659668334,-4.768341939498,336.205030377428));
#53939=CARTESIAN_POINT('Ctrl Pts',(129.764801763724,-4.73428379744144,336.339799483827));
#53940=CARTESIAN_POINT('Ctrl Pts',(129.756943859115,-4.69448163524061,336.473225839371));
#53941=CARTESIAN_POINT('Ctrl Pts',(129.749085954506,-4.64907069308588,336.60478183975));
#53942=CARTESIAN_POINT('Ctrl Pts',(129.741416910387,-4.60475117838075,336.733175962766));
#53943=CARTESIAN_POINT('Ctrl Pts',(129.733747866268,-4.55508957025285,336.859788217815));
#53944=CARTESIAN_POINT('Ctrl Pts',(129.726078822148,-4.50026218666953,336.98414296706));
#53945=CARTESIAN_POINT('Ctrl Pts',(129.71841056241,-4.44544041076472,337.108484997451));
#53946=CARTESIAN_POINT('Ctrl Pts',(129.710742302671,-4.38545407126322,337.230569615472));
#53947=CARTESIAN_POINT('Ctrl Pts',(129.703074042932,-4.32052742086686,337.349941673327));
#53948=CARTESIAN_POINT('Ctrl Pts',(129.695404824386,-4.25559265230907,337.469328656972));
#53949=CARTESIAN_POINT('Ctrl Pts',(129.68773560584,-4.18571653553597,337.586002054872));
#53950=CARTESIAN_POINT('Ctrl Pts',(129.680066387293,-4.11116875989336,337.699532272483));
#53951=CARTESIAN_POINT('Ctrl Pts',(129.672066684828,-4.0334085525173,337.817954763144));
#53952=CARTESIAN_POINT('Ctrl Pts',(129.664066982363,-3.95056533088207,337.932956728345));
#53953=CARTESIAN_POINT('Ctrl Pts',(129.656067279898,-3.86299387396652,338.044086298415));
#53954=CARTESIAN_POINT('Ctrl Pts',(129.648386724832,-3.7789160723258,338.150782364438));
#53955=CARTESIAN_POINT('Ctrl Pts',(129.640706169766,-3.69048034393063,338.25390879637));
#53956=CARTESIAN_POINT('Ctrl Pts',(129.6330256147,-3.59803973352374,338.353102017309));
#53957=CARTESIAN_POINT('Ctrl Pts',(129.625339857815,-3.50553651575038,338.452362418964));
#53958=CARTESIAN_POINT('Ctrl Pts',(129.61765410093,-3.40902329967104,338.547684026976));
#53959=CARTESIAN_POINT('Ctrl Pts',(129.609968344045,-3.30888767288203,338.638742286938));
#53960=CARTESIAN_POINT('Ctrl Pts',(129.602272103373,-3.20861545569685,338.729924755278));
#53961=CARTESIAN_POINT('Ctrl Pts',(129.594575862701,-3.10471127504674,338.816832019167));
#53962=CARTESIAN_POINT('Ctrl Pts',(129.586879622029,-2.99759335683159,338.89918159741));
#53963=CARTESIAN_POINT('Ctrl Pts',(129.585943067257,-2.98455818787116,338.909202709509));
#53964=CARTESIAN_POINT('Ctrl Pts',(129.585006512484,-2.97147546006877,338.919156384379));
#53965=CARTESIAN_POINT('Ctrl Pts',(129.584069957712,-2.95834595254926,338.929042159043));
#53966=CARTESIAN_POINT('Ctrl Pts',(129.576294878933,-2.84934757008491,339.011111760372));
#53967=CARTESIAN_POINT('Ctrl Pts',(129.568519800155,-2.73675923381156,339.088771907027));
#53968=CARTESIAN_POINT('Ctrl Pts',(129.560744721376,-2.62097331088899,339.161692199828));
#53969=CARTESIAN_POINT('Ctrl Pts',(129.552979210327,-2.50532986991576,339.234522759566));
#53970=CARTESIAN_POINT('Ctrl Pts',(129.545213699278,-2.38649699907022,339.302624864524));
#53971=CARTESIAN_POINT('Ctrl Pts',(129.537448188229,-2.26489932397997,339.365708890287));
#53972=CARTESIAN_POINT('Ctrl Pts',(129.529690376707,-2.14342221333894,339.428730368055));
#53973=CARTESIAN_POINT('Ctrl Pts',(129.521932565185,-2.01918609854448,339.486743489193));
#53974=CARTESIAN_POINT('Ctrl Pts',(129.514174753663,-1.89264341481996,339.539502612274));
#53975=CARTESIAN_POINT('Ctrl Pts',(129.50642278014,-1.76619595847742,339.592222032441));
#53976=CARTESIAN_POINT('Ctrl Pts',(129.498670806617,-1.63744574748366,339.639695174586));
#53977=CARTESIAN_POINT('Ctrl Pts',(129.490918833094,-1.50686825842056,339.681723092438));
#53978=CARTESIAN_POINT('Ctrl Pts',(129.483170142536,-1.37634606900174,339.723733211441));
#53979=CARTESIAN_POINT('Ctrl Pts',(129.475421451978,-1.24399851195549,339.760302573226));
#53980=CARTESIAN_POINT('Ctrl Pts',(129.467672761421,-1.11031920741886,339.791281072963));
#53981=CARTESIAN_POINT('Ctrl Pts',(129.459925683043,-0.97666771597813,339.822253127365));
#53982=CARTESIAN_POINT('Ctrl Pts',(129.452178604665,-0.841685408725561,
339.847636545272));
#53983=CARTESIAN_POINT('Ctrl Pts',(129.444431526287,-0.7058787838073,339.867331733617));
#53984=CARTESIAN_POINT('Ctrl Pts',(129.436684382981,-0.570071020698901,
339.887027087026));
#53985=CARTESIAN_POINT('Ctrl Pts',(129.428937239676,-0.433439312972735,
339.901034059688));
#53986=CARTESIAN_POINT('Ctrl Pts',(129.42119009637,-0.296497621167412,339.909304657805));
#53987=CARTESIAN_POINT('Ctrl Pts',(129.413441211342,-0.159525141962369,
339.917577115328));
#53988=CARTESIAN_POINT('Ctrl Pts',(129.405692326314,-0.0222429300879784,
339.92011060847));
#53989=CARTESIAN_POINT('Ctrl Pts',(129.397943441285,0.114833093437252,339.916909234789));
#53990=CARTESIAN_POINT('Ctrl Pts',(129.390186331511,0.252054610870299,339.913704463136));
#53991=CARTESIAN_POINT('Ctrl Pts',(129.382429221736,0.389069111394956,339.904752674354));
#53992=CARTESIAN_POINT('Ctrl Pts',(129.374672111961,0.525363284476724,339.890110068477));
#53993=CARTESIAN_POINT('Ctrl Pts',(129.366910857035,0.661730288806791,339.875459638061));
#53994=CARTESIAN_POINT('Ctrl Pts',(129.359149602109,0.797375812352754,339.855112389056));
#53995=CARTESIAN_POINT('Ctrl Pts',(129.351388347183,0.931795793713294,339.829175878068));
#53996=CARTESIAN_POINT('Ctrl Pts',(129.343614676778,1.06643080323655,339.803197877116));
#53997=CARTESIAN_POINT('Ctrl Pts',(129.335841006373,1.19983597241944,339.77161283752));
#53998=CARTESIAN_POINT('Ctrl Pts',(129.328067335969,1.33152061665565,339.734578746829));
#53999=CARTESIAN_POINT('Ctrl Pts',(129.320655531791,1.45707530902113,339.699268601968));
#54000=CARTESIAN_POINT('Ctrl Pts',(129.313243727614,1.58106577881586,339.659005384936));
#54001=CARTESIAN_POINT('Ctrl Pts',(129.305831923437,1.70308462919649,339.613966385692));
#54002=CARTESIAN_POINT('Ctrl Pts',(129.298056844659,1.83108398690973,339.566719890931));
#54003=CARTESIAN_POINT('Ctrl Pts',(129.29028176588,1.9573180701139,339.514068318486));
#54004=CARTESIAN_POINT('Ctrl Pts',(129.282506687102,2.08129670670435,339.456162820315));
#54005=CARTESIAN_POINT('Ctrl Pts',(129.274741176053,2.20512277968961,339.398328578547));
#54006=CARTESIAN_POINT('Ctrl Pts',(129.266975665004,2.3266985776872,339.335253438956));
#54007=CARTESIAN_POINT('Ctrl Pts',(129.259210153955,2.44555076005456,339.267137745901));
#54008=CARTESIAN_POINT('Ctrl Pts',(129.251452342433,2.56428510013716,339.199089589755));
#54009=CARTESIAN_POINT('Ctrl Pts',(129.24369453091,2.68030086174008,339.126011019002));
#54010=CARTESIAN_POINT('Ctrl Pts',(129.235936719388,2.79314664108628,339.048149565405));
#54011=CARTESIAN_POINT('Ctrl Pts',(129.228184745865,2.90590750040521,338.970346705021));
#54012=CARTESIAN_POINT('Ctrl Pts',(129.220432772342,3.01550280528449,338.887768347053));
#54013=CARTESIAN_POINT('Ctrl Pts',(129.212680798819,3.12150794989926,338.800706668663));
#54014=CARTESIAN_POINT('Ctrl Pts',(129.204932108261,3.2274682012721,338.713681860944));
#54015=CARTESIAN_POINT('Ctrl Pts',(129.197183417704,3.32984101498881,338.622177756724));
#54016=CARTESIAN_POINT('Ctrl Pts',(129.189434727146,3.42823303851712,338.52652822137));
#54017=CARTESIAN_POINT('Ctrl Pts',(129.181687648768,3.52660459076311,338.430898586701));
#54018=CARTESIAN_POINT('Ctrl Pts',(129.173940570391,3.62099672014969,338.33112550874));
#54019=CARTESIAN_POINT('Ctrl Pts',(129.166193492013,3.71105158153307,338.227581017062));
#54020=CARTESIAN_POINT('Ctrl Pts',(129.158446348707,3.80110719766293,338.124035657582));
#54021=CARTESIAN_POINT('Ctrl Pts',(129.150699205401,3.88682521677621,338.016719116272));
#54022=CARTESIAN_POINT('Ctrl Pts',(129.142952062095,3.96788714632693,337.906037621318));
#54023=CARTESIAN_POINT('Ctrl Pts',(129.135203177067,4.04896730032052,337.795331242813));
#54024=CARTESIAN_POINT('Ctrl Pts',(129.127454292039,4.12538905085071,337.681258720571));
#54025=CARTESIAN_POINT('Ctrl Pts',(129.119705407011,4.19687664917404,337.564256121006));
#54026=CARTESIAN_POINT('Ctrl Pts',(129.111948297236,4.26844012517271,337.447129333673));
#54027=CARTESIAN_POINT('Ctrl Pts',(129.104191187462,4.33505878313159,337.327066590542));
#54028=CARTESIAN_POINT('Ctrl Pts',(129.096434077687,4.39650210107624,337.204529958456));
#54029=CARTESIAN_POINT('Ctrl Pts',(129.088672822761,4.45797825236537,337.081927846713));
#54030=CARTESIAN_POINT('Ctrl Pts',(129.080911567834,4.51427339271712,336.956849568132));
#54031=CARTESIAN_POINT('Ctrl Pts',(129.073150312908,4.56520519222738,336.829777203749));
#54032=CARTESIAN_POINT('Ctrl Pts',(129.065376642504,4.61621846601826,336.702501564996));
#54033=CARTESIAN_POINT('Ctrl Pts',(129.057602972099,4.66185112421688,336.573225834882));
#54034=CARTESIAN_POINT('Ctrl Pts',(129.049829301694,4.70197048432592,336.442448136686));
#54035=CARTESIAN_POINT('Ctrl Pts',(129.042417497517,4.7402222785698,336.317758171804));
#54036=CARTESIAN_POINT('Ctrl Pts',(129.03500569334,4.77346243816642,336.191703203493));
#54037=CARTESIAN_POINT('Ctrl Pts',(129.027593889163,4.80161958421862,336.064721762222));
#54038=CARTESIAN_POINT('Ctrl Pts',(129.019818810385,4.83115679587456,335.931516582256));
#54039=CARTESIAN_POINT('Ctrl Pts',(129.012043731606,4.85519347106497,335.796870861606));
#54040=CARTESIAN_POINT('Ctrl Pts',(129.004268652828,4.87359145644578,335.661278593453));
#54041=CARTESIAN_POINT('Ctrl Pts',(128.996503141779,4.89196680193436,335.525853180217));
#54042=CARTESIAN_POINT('Ctrl Pts',(128.98873763073,4.90471721171743,335.389483920691));
#54043=CARTESIAN_POINT('Ctrl Pts',(128.980972119681,4.91175500785868,335.252677274948));
#54044=CARTESIAN_POINT('Ctrl Pts',(128.973214308159,4.91878582600455,335.116006273393));
#54045=CARTESIAN_POINT('Ctrl Pts',(128.965456496636,4.92011528238229,334.978899136492));
#54046=CARTESIAN_POINT('Ctrl Pts',(128.957698685114,4.91570725124464,334.84186941295));
#54047=CARTESIAN_POINT('Ctrl Pts',(128.949946711591,4.91130253729023,334.704942808621));
#54048=CARTESIAN_POINT('Ctrl Pts',(128.942194738068,4.90116894239111,334.568093890794));
#54049=CARTESIAN_POINT('Ctrl Pts',(128.934442764545,4.88532238597772,334.431837833392));
#54050=CARTESIAN_POINT('Ctrl Pts',(128.926694073988,4.86948254059035,334.295639480511));
#54051=CARTESIAN_POINT('Ctrl Pts',(128.91894538343,4.84793459084983,334.16003387613));
#54052=CARTESIAN_POINT('Ctrl Pts',(128.911196692872,4.82074642564162,334.025532472494));
#54053=CARTESIAN_POINT('Ctrl Pts',(128.903449614495,4.79356391715833,333.891059052999));
#54054=CARTESIAN_POINT('Ctrl Pts',(128.895702536117,4.76074360476628,333.757689760168));
#54055=CARTESIAN_POINT('Ctrl Pts',(128.887955457739,4.72240468553071,333.625926840166));
#54056=CARTESIAN_POINT('Ctrl Pts',(128.880208314433,4.6840654449781,333.494162815863));
#54057=CARTESIAN_POINT('Ctrl Pts',(128.872461171127,4.64020761453386,333.364005566553));
#54058=CARTESIAN_POINT('Ctrl Pts',(128.864714027822,4.59100044555316,333.235942752791));
#54059=CARTESIAN_POINT('Ctrl Pts',(128.856965142794,4.5417822137561,333.107851147789));
#54060=CARTESIAN_POINT('Ctrl Pts',(128.849216257766,4.48721239046338,332.981855280117));
#54061=CARTESIAN_POINT('Ctrl Pts',(128.841467372737,4.42750844975837,332.858423013334));
#54062=CARTESIAN_POINT('Ctrl Pts',(128.833710262963,4.36774113867383,332.734859734267));
#54063=CARTESIAN_POINT('Ctrl Pts',(128.825953153188,4.30282899494784,332.613865844036));
#54064=CARTESIAN_POINT('Ctrl Pts',(128.818196043413,4.23303583177944,332.495885244368));
#54065=CARTESIAN_POINT('Ctrl Pts',(128.810434788487,4.16320537337622,332.377841599641));
#54066=CARTESIAN_POINT('Ctrl Pts',(128.802673533561,4.08848891114797,332.262814781585));
#54067=CARTESIAN_POINT('Ctrl Pts',(128.794912278635,4.00919316814962,332.151218997016));
#54068=CARTESIAN_POINT('Ctrl Pts',(128.78713860823,3.92977057780487,332.039444695561));
#54069=CARTESIAN_POINT('Ctrl Pts',(128.779364937826,3.84575430812722,331.931112704347));
#54070=CARTESIAN_POINT('Ctrl Pts',(128.771591267421,3.75749143949776,331.826604162005));
#54071=CARTESIAN_POINT('Ctrl Pts',(128.764179463244,3.67333722863829,331.726960517454));
#54072=CARTESIAN_POINT('Ctrl Pts',(128.756767659067,3.58532307419928,331.630792581717));
#54073=CARTESIAN_POINT('Ctrl Pts',(128.74935585489,3.49377911859015,331.53839769283));
#54074=CARTESIAN_POINT('Ctrl Pts',(128.741580776111,3.3977483210208,331.441474255209));
#54075=CARTESIAN_POINT('Ctrl Pts',(128.733805697333,3.29752948615606,331.348396776828));
#54076=CARTESIAN_POINT('Ctrl Pts',(128.726030618555,3.1934632606972,331.259548761837));
#54077=CARTESIAN_POINT('Ctrl Pts',(128.718265107506,3.08952509535413,331.170810079984));
#54078=CARTESIAN_POINT('Ctrl Pts',(128.710499596457,2.98174925406078,331.086290757184));
#54079=CARTESIAN_POINT('Ctrl Pts',(128.702734085408,2.87051418233513,331.006338598289));
#54080=CARTESIAN_POINT('Ctrl Pts',(128.694976273886,2.75938940050737,330.926465712193));
#54081=CARTESIAN_POINT('Ctrl Pts',(128.687218462363,2.64481252916569,330.85115120498));
#54082=CARTESIAN_POINT('Ctrl Pts',(128.679460650841,2.52719587265771,330.780703366233));
#54083=CARTESIAN_POINT('Ctrl Pts',(128.671708677318,2.40966772641242,330.710308541717));
#54084=CARTESIAN_POINT('Ctrl Pts',(128.663956703795,2.28910468220214,330.644773296033));
#54085=CARTESIAN_POINT('Ctrl Pts',(128.656204730272,2.16594857568623,330.584363032361));
#54086=CARTESIAN_POINT('Ctrl Pts',(128.648456039714,2.04284462585513,330.523978352471));
#54087=CARTESIAN_POINT('Ctrl Pts',(128.640707349157,1.91715014808726,330.468714509535));
#54088=CARTESIAN_POINT('Ctrl Pts',(128.632958658599,1.78933197205771,330.418791190497));
#54089=CARTESIAN_POINT('Ctrl Pts',(128.625211580221,1.66154038966724,330.368878258421));
#54090=CARTESIAN_POINT('Ctrl Pts',(128.617464501844,1.53162635175188,330.324303782223));
#54091=CARTESIAN_POINT('Ctrl Pts',(128.609717423466,1.40007671219846,330.285239320765));
#54092=CARTESIAN_POINT('Ctrl Pts',(128.60197028016,1.26852597013235,330.246174531909));
#54093=CARTESIAN_POINT('Ctrl Pts',(128.594223136854,1.13533997378885,330.212619961172));
#54094=CARTESIAN_POINT('Ctrl Pts',(128.586475993548,1.00102039895376,330.184697182588));
#54095=CARTESIAN_POINT('Ctrl Pts',(128.57872710852,0.866670626226927,330.15676812637));
#54096=CARTESIAN_POINT('Ctrl Pts',(128.570978223492,0.731187150498339,330.134473461334));
#54097=CARTESIAN_POINT('Ctrl Pts',(128.563229338464,0.595081095921843,330.117883496702));
#54098=CARTESIAN_POINT('Ctrl Pts',(128.555472228689,0.458830576972364,330.10127592331));
#54099=CARTESIAN_POINT('Ctrl Pts',(128.547715118915,0.321956547757211,330.090385193177));
#54100=CARTESIAN_POINT('Ctrl Pts',(128.53995800914,0.184975059170039,330.085229680851));
#54101=CARTESIAN_POINT('Ctrl Pts',(128.532196754214,0.0479203720552305,
330.080071413585));
#54102=CARTESIAN_POINT('Ctrl Pts',(128.524435499288,-0.0892414981793248,
330.080654469191));
#54103=CARTESIAN_POINT('Ctrl Pts',(128.516674244361,-0.22599625073994,330.086945068783));
#54104=CARTESIAN_POINT('Ctrl Pts',(128.508900573957,-0.362969766336476,
330.093245731285));
#54105=CARTESIAN_POINT('Ctrl Pts',(128.501126903552,-0.499534473285334,
330.105272148331));
#54106=CARTESIAN_POINT('Ctrl Pts',(128.493353233147,-0.635182038869866,
330.122938708608));
#54107=CARTESIAN_POINT('Ctrl Pts',(128.48594142897,-0.764515177642398,330.139782886253));
#54108=CARTESIAN_POINT('Ctrl Pts',(128.478529624793,-0.893014355676524,
330.161753878278));
#54109=CARTESIAN_POINT('Ctrl Pts',(128.471117820616,-1.02025087607247,330.188734967561));
#54110=CARTESIAN_POINT('Ctrl Pts',(128.463342741838,-1.15372363734993,330.217038480401));
#54111=CARTESIAN_POINT('Ctrl Pts',(128.455567663059,-1.28622863674198,330.250945072378));
#54112=CARTESIAN_POINT('Ctrl Pts',(128.447792584281,-1.41725903395184,330.290375822512));
#54113=CARTESIAN_POINT('Ctrl Pts',(128.440027073232,-1.54812818991649,330.329758050598));
#54114=CARTESIAN_POINT('Ctrl Pts',(128.432261562183,-1.67752598350064,330.374650799553));
#54115=CARTESIAN_POINT('Ctrl Pts',(128.424496051134,-1.80495513959806,330.424924043632));
#54116=CARTESIAN_POINT('Ctrl Pts',(128.416738239611,-1.93225794931522,330.475147441642));
#54117=CARTESIAN_POINT('Ctrl Pts',(128.408980428089,-2.05759564469798,330.530740575745));
#54118=CARTESIAN_POINT('Ctrl Pts',(128.401222616567,-2.18048585691809,330.591523563602));
#54119=CARTESIAN_POINT('Ctrl Pts',(128.393470643044,-2.30328359035696,330.652260810333));
#54120=CARTESIAN_POINT('Ctrl Pts',(128.385718669521,-2.42363715771364,330.718179964457));
#54121=CARTESIAN_POINT('Ctrl Pts',(128.377966695998,-2.54108427316294,330.789053101833));
#54122=CARTESIAN_POINT('Ctrl Pts',(128.370218005441,-2.65848164968912,330.859896224393));
#54123=CARTESIAN_POINT('Ctrl Pts',(128.362469314883,-2.77297468848427,330.935688955871));
#54124=CARTESIAN_POINT('Ctrl Pts',(128.354720624325,-2.88412602178613,331.016157614444));
#54125=CARTESIAN_POINT('Ctrl Pts',(128.346973545947,-2.99525422912493,331.09660953084));
#54126=CARTESIAN_POINT('Ctrl Pts',(128.33922646757,-3.10304179749696,331.181735210164));
#54127=CARTESIAN_POINT('Ctrl Pts',(128.331479389192,-3.20708099481977,331.27121808694));
#54128=CARTESIAN_POINT('Ctrl Pts',(128.323732245886,-3.31112106409162,331.360701713668));
#54129=CARTESIAN_POINT('Ctrl Pts',(128.31598510258,-3.41141240331253,331.454542355806));
#54130=CARTESIAN_POINT('Ctrl Pts',(128.308237959274,-3.50758129272998,331.552383934167));
#54131=CARTESIAN_POINT('Ctrl Pts',(128.300489074246,-3.60377180295506,331.650247509391));
#54132=CARTESIAN_POINT('Ctrl Pts',(128.292740189218,-3.69583774517671,331.752113532026));
#54133=CARTESIAN_POINT('Ctrl Pts',(128.28499130419,-3.78344339626242,331.857590235221));
#54134=CARTESIAN_POINT('Ctrl Pts',(128.277234194415,-3.87114203289136,331.963178892478));
#54135=CARTESIAN_POINT('Ctrl Pts',(128.26947708464,-3.95437067124238,332.072385584739));
#54136=CARTESIAN_POINT('Ctrl Pts',(128.261719974866,-4.03283459501543,332.184786297322));
#54137=CARTESIAN_POINT('Ctrl Pts',(128.25395871994,-4.11134044740058,332.297247073251));
#54138=CARTESIAN_POINT('Ctrl Pts',(128.246197465013,-4.18507630183322,332.412904940996));
#54139=CARTESIAN_POINT('Ctrl Pts',(128.238436210087,-4.25379224602821,332.531309134353));
#54140=CARTESIAN_POINT('Ctrl Pts',(128.230662539683,-4.32261811333938,332.649902735831));
#54141=CARTESIAN_POINT('Ctrl Pts',(128.222888869278,-4.38640784168429,332.771251095724));
#54142=CARTESIAN_POINT('Ctrl Pts',(128.215115198873,-4.44495833544178,332.89488041701));
#54143=CARTESIAN_POINT('Ctrl Pts',(128.207703394696,-4.50078328962875,333.012754763648));
#54144=CARTESIAN_POINT('Ctrl Pts',(128.200291590519,-4.55184569221968,333.132702228346));
#54145=CARTESIAN_POINT('Ctrl Pts',(128.192879786342,-4.59801170064182,333.254299148405));
#54146=CARTESIAN_POINT('Ctrl Pts',(128.183991545777,-4.6533740090564,333.400118256892));
#54147=CARTESIAN_POINT('Ctrl Pts',(128.175103305213,-4.70184091569508,333.548691672308));
#54148=CARTESIAN_POINT('Ctrl Pts',(128.166215064648,-4.74316593011621,333.699400129984));
#54149=CARTESIAN_POINT('Ctrl Pts',(128.15735782075,-4.78434682853533,333.849583010097));
#54150=CARTESIAN_POINT('Ctrl Pts',(128.148500576852,-4.81843545617234,334.001885917024));
#54151=CARTESIAN_POINT('Ctrl Pts',(128.139643332954,-4.84523439894587,334.155673829748));
#54152=CARTESIAN_POINT('Ctrl Pts',(128.130845505093,-4.87185356943344,334.308430104589));
#54153=CARTESIAN_POINT('Ctrl Pts',(128.122047677233,-4.89128044364123,334.462651363844));
#54154=CARTESIAN_POINT('Ctrl Pts',(128.113249849372,-4.90336889032551,334.617695686804));
#54155=CARTESIAN_POINT('Ctrl Pts',(128.106105691769,-4.91318515061795,334.743597340738));
#54156=CARTESIAN_POINT('Ctrl Pts',(128.098961534166,-4.91816327654134,334.870041323959));
#54157=CARTESIAN_POINT('Ctrl Pts',(128.091817376563,-4.91824887636649,334.996675451945));
#54158=CARTESIAN_POINT('',(126.341816235661,-4.91546218483043,335.003626104507));
#54159=CARTESIAN_POINT('Ctrl Pts',(128.091817376508,-4.91824887636714,334.996675452912));
#54160=CARTESIAN_POINT('Ctrl Pts',(128.084031730335,-4.9183421623491,335.134680319095));
#54161=CARTESIAN_POINT('Ctrl Pts',(128.076246084161,-4.91262254950206,335.272721930806));
#54162=CARTESIAN_POINT('Ctrl Pts',(128.068460437988,-4.90110745943531,335.41027884855));
#54163=CARTESIAN_POINT('Ctrl Pts',(128.060674700231,-4.88959223391519,335.547837384393));
#54164=CARTESIAN_POINT('Ctrl Pts',(128.052888962474,-4.87228142675415,335.684910830953));
#54165=CARTESIAN_POINT('Ctrl Pts',(128.045103224717,-4.84924442610522,335.820982069468));
#54166=CARTESIAN_POINT('Ctrl Pts',(128.03731577343,-4.82620235534134,335.95708325532));
#54167=CARTESIAN_POINT('Ctrl Pts',(128.029528322144,-4.79743164625134,336.092181414168));
#54168=CARTESIAN_POINT('Ctrl Pts',(128.021740870857,-4.76305291408951,336.225769146325));
#54169=CARTESIAN_POINT('Ctrl Pts',(128.013950083339,-4.72865945369409,336.359414108962));
#54170=CARTESIAN_POINT('Ctrl Pts',(128.006159295821,-4.68865328308514,336.491546983912));
#54171=CARTESIAN_POINT('Ctrl Pts',(127.998368508303,-4.64320493090818,336.621675378148));
#54172=CARTESIAN_POINT('Ctrl Pts',(127.990567897971,-4.5976992763457,336.751967841421));
#54173=CARTESIAN_POINT('Ctrl Pts',(127.982767287639,-4.54673786409452,336.880250412829));
#54174=CARTESIAN_POINT('Ctrl Pts',(127.974966677307,-4.49053968726436,337.006049944444));
#54175=CARTESIAN_POINT('Ctrl Pts',(127.967160619224,-4.43430226303195,337.131937331308));
#54176=CARTESIAN_POINT('Ctrl Pts',(127.959354561141,-4.37282095856092,337.255337879206));
#54177=CARTESIAN_POINT('Ctrl Pts',(127.951548503058,-4.30636039055699,337.375803705937));
#54178=CARTESIAN_POINT('Ctrl Pts',(127.943729882914,-4.23979286951245,337.496463394785));
#54179=CARTESIAN_POINT('Ctrl Pts',(127.935911262771,-4.16823027956881,337.614178600881));
#54180=CARTESIAN_POINT('Ctrl Pts',(127.928092642628,-4.09198055196934,337.728530414858));
#54181=CARTESIAN_POINT('Ctrl Pts',(127.923609012441,-4.04825473153978,337.794106083666));
#54182=CARTESIAN_POINT('Ctrl Pts',(127.919125382254,-4.00298829587374,337.85857629584));
#54183=CARTESIAN_POINT('Ctrl Pts',(127.914641752068,-3.95624505407418,337.921867234255));
#54184=CARTESIAN_POINT('Ctrl Pts',(127.906866673289,-3.87518743508755,338.031620271782));
#54185=CARTESIAN_POINT('Ctrl Pts',(127.899091594511,-3.78943116206288,338.138171167979));
#54186=CARTESIAN_POINT('Ctrl Pts',(127.891316515732,-3.69925804687033,338.241091323176));
#54187=CARTESIAN_POINT('Ctrl Pts',(127.883551004683,-3.60919589543658,338.343884828569));
#54188=CARTESIAN_POINT('Ctrl Pts',(127.875785493634,-3.51472797145635,338.443056191533));
#54189=CARTESIAN_POINT('Ctrl Pts',(127.868019982585,-3.41617863654083,338.538206690647));
#54190=CARTESIAN_POINT('Ctrl Pts',(127.860262171063,-3.31772701357783,338.633262847764));
#54191=CARTESIAN_POINT('Ctrl Pts',(127.852504359541,-3.21520231228766,338.724305805037));
#54192=CARTESIAN_POINT('Ctrl Pts',(127.844746548019,-3.10896809520671,338.810971063323));
#54193=CARTESIAN_POINT('Ctrl Pts',(127.836994574496,-3.00281382274318,338.897571103254));
#54194=CARTESIAN_POINT('Ctrl Pts',(127.829242600973,-2.89295589254402,338.979799755368));
#54195=CARTESIAN_POINT('Ctrl Pts',(127.82149062745,-2.77979327165223,339.057330702491));
#54196=CARTESIAN_POINT('Ctrl Pts',(127.813741936892,-2.66667857519761,339.134828815212));
#54197=CARTESIAN_POINT('Ctrl Pts',(127.805993246334,-2.55026229341606,339.207632959419));
#54198=CARTESIAN_POINT('Ctrl Pts',(127.798244555777,-2.43097471582919,339.275458454189));
#54199=CARTESIAN_POINT('Ctrl Pts',(127.790497477399,-2.31171195701911,339.343269837299));
#54200=CARTESIAN_POINT('Ctrl Pts',(127.782750399021,-2.18957943024431,339.406104438273));
#54201=CARTESIAN_POINT('Ctrl Pts',(127.775003320643,-2.06503417723717,339.463722315438));
#54202=CARTESIAN_POINT('Ctrl Pts',(127.767256177337,-1.94048788042103,339.521340675497));
#54203=CARTESIAN_POINT('Ctrl Pts',(127.759509034032,-1.81352917179135,339.573742060426));
#54204=CARTESIAN_POINT('Ctrl Pts',(127.751761890726,-1.6846369649321,339.620733855015));
#54205=CARTESIAN_POINT('Ctrl Pts',(127.744013005698,-1.55571578036802,339.667736214358));
#54206=CARTESIAN_POINT('Ctrl Pts',(127.73626412067,-1.42486059974457,339.709326429418));
#54207=CARTESIAN_POINT('Ctrl Pts',(127.728515235641,-1.29256707557367,339.745361252596));
#54208=CARTESIAN_POINT('Ctrl Pts',(127.720758125867,-1.16013313368955,339.781434323508));
#54209=CARTESIAN_POINT('Ctrl Pts',(127.713001016092,-1.02625817631579,339.811940120738));
#54210=CARTESIAN_POINT('Ctrl Pts',(127.705243906317,-0.891450217033445,
339.836786078901));
#54211=CARTESIAN_POINT('Ctrl Pts',(127.697482651391,-0.756570220688029,
339.86164531395));
#54212=CARTESIAN_POINT('Ctrl Pts',(127.689721396465,-0.620756615827872,
339.880838628801));
#54213=CARTESIAN_POINT('Ctrl Pts',(127.681960141539,-0.484523201517907,
339.894325319152));
#54214=CARTESIAN_POINT('Ctrl Pts',(127.674186471134,-0.348071858143504,
339.907833583812));
#54215=CARTESIAN_POINT('Ctrl Pts',(127.66641280073,-0.211199753796001,339.915616959843));
#54216=CARTESIAN_POINT('Ctrl Pts',(127.658639130325,-0.0744222528240178,
339.917686894342));
#54217=CARTESIAN_POINT('Ctrl Pts',(127.651227326148,0.055988222569004,339.919660472892));
#54218=CARTESIAN_POINT('Ctrl Pts',(127.643815521971,0.186312416243332,339.916440567866));
#54219=CARTESIAN_POINT('Ctrl Pts',(127.636403717794,0.316109284535064,339.90808088592));
#54220=CARTESIAN_POINT('Ctrl Pts',(127.628628639016,0.452267883988871,339.899311471059));
#54221=CARTESIAN_POINT('Ctrl Pts',(127.620853560237,0.588276445791939,339.884857995364));
#54222=CARTESIAN_POINT('Ctrl Pts',(127.613078481459,0.723622046764772,339.864725500574));
#54223=CARTESIAN_POINT('Ctrl Pts',(127.60531297041,0.858801096358901,339.8446177801));
#54224=CARTESIAN_POINT('Ctrl Pts',(127.597547459361,0.9933184254372,339.818845002392));
#54225=CARTESIAN_POINT('Ctrl Pts',(127.589781948312,1.12666320997102,339.787464159009));
#54226=CARTESIAN_POINT('Ctrl Pts',(127.582024136789,1.25987578276284,339.756114429824));
#54227=CARTESIAN_POINT('Ctrl Pts',(127.574266325267,1.39191774658354,339.719167789464));
#54228=CARTESIAN_POINT('Ctrl Pts',(127.566508513745,1.52228584177884,339.676732714024));
#54229=CARTESIAN_POINT('Ctrl Pts',(127.558756540222,1.65255583084842,339.634329572323));
#54230=CARTESIAN_POINT('Ctrl Pts',(127.551004566699,1.78115408835958,339.58644633704));
#54231=CARTESIAN_POINT('Ctrl Pts',(127.543252593176,1.90759030328039,339.533241919127));
#54232=CARTESIAN_POINT('Ctrl Pts',(127.535503902618,2.03397297238907,339.480060033317));
#54233=CARTESIAN_POINT('Ctrl Pts',(127.527755212061,2.15819506049739,339.421561598265));
#54234=CARTESIAN_POINT('Ctrl Pts',(127.520006521503,2.27978431899547,339.35795439643));
#54235=CARTESIAN_POINT('Ctrl Pts',(127.512259443125,2.4013482798327,339.294360428604));
#54236=CARTESIAN_POINT('Ctrl Pts',(127.504512364748,2.52028015450945,339.225659989292));
#54237=CARTESIAN_POINT('Ctrl Pts',(127.49676528637,2.63613083944876,339.152107568429));
#54238=CARTESIAN_POINT('Ctrl Pts',(127.489018143064,2.75198249532831,339.078554531127));
#54239=CARTESIAN_POINT('Ctrl Pts',(127.481270999758,2.86475257997815,339.000149640671));
#54240=CARTESIAN_POINT('Ctrl Pts',(127.473523856452,2.97401995153915,338.917191390569));
#54241=CARTESIAN_POINT('Ctrl Pts',(127.465774971424,3.08331188872535,338.834214489691));
#54242=CARTESIAN_POINT('Ctrl Pts',(127.458026086396,3.18909923456191,338.746682428447));
#54243=CARTESIAN_POINT('Ctrl Pts',(127.450277201368,3.29099330307165,338.654934492113));
#54244=CARTESIAN_POINT('Ctrl Pts',(127.442520091593,3.39299552299822,338.563089173571));
#54245=CARTESIAN_POINT('Ctrl Pts',(127.434762981818,3.49109591987966,338.467019303122));
#54246=CARTESIAN_POINT('Ctrl Pts',(127.427005872044,3.58494173821103,338.367101987783));
#54247=CARTESIAN_POINT('Ctrl Pts',(127.419244617118,3.6788377047472,338.267131279825));
#54248=CARTESIAN_POINT('Ctrl Pts',(127.411483362191,3.76847430725011,338.16330932602));
#54249=CARTESIAN_POINT('Ctrl Pts',(127.403722107265,3.8535392704469,338.05604616353));
#54250=CARTESIAN_POINT('Ctrl Pts',(127.395948436861,3.93874030986212,337.948611414936));
#54251=CARTESIAN_POINT('Ctrl Pts',(127.388174766456,4.01935486620013,337.837724773732));
#54252=CARTESIAN_POINT('Ctrl Pts',(127.380401096051,4.09511367234788,337.723825815475));
#54253=CARTESIAN_POINT('Ctrl Pts',(127.372989291874,4.16734588784317,337.615228881127));
#54254=CARTESIAN_POINT('Ctrl Pts',(127.365577487697,4.23516410021169,337.503894010952));
#54255=CARTESIAN_POINT('Ctrl Pts',(127.35816568352,4.29837479849395,337.390221151729));
#54256=CARTESIAN_POINT('Ctrl Pts',(127.350390604741,4.36468364139377,337.270976847062));
#54257=CARTESIAN_POINT('Ctrl Pts',(127.342615525963,4.42613144229161,337.148782740788));
#54258=CARTESIAN_POINT('Ctrl Pts',(127.334840447185,4.48244486872974,337.024072889324));
#54259=CARTESIAN_POINT('Ctrl Pts',(127.327074936136,4.53868899791155,336.899516501273));
#54260=CARTESIAN_POINT('Ctrl Pts',(127.319309425087,4.58981116466563,336.77245088059));
#54261=CARTESIAN_POINT('Ctrl Pts',(127.311543914038,4.63558285821723,336.643336431502));
#54262=CARTESIAN_POINT('Ctrl Pts',(127.303786102515,4.68130916900118,336.514349999767));
#54263=CARTESIAN_POINT('Ctrl Pts',(127.296028290993,4.72169543409043,336.383319148303));
#54264=CARTESIAN_POINT('Ctrl Pts',(127.288270479471,4.75656053066944,336.250725781528));
#54265=CARTESIAN_POINT('Ctrl Pts',(127.280518505948,4.79139939015789,336.118232195464));
#54266=CARTESIAN_POINT('Ctrl Pts',(127.272766532425,4.82072525217029,335.984178811048));
#54267=CARTESIAN_POINT('Ctrl Pts',(127.265014558902,4.84440641288281,335.849063937121));
#54268=CARTESIAN_POINT('Ctrl Pts',(127.257265868344,4.86807754460964,335.714006284424));
#54269=CARTESIAN_POINT('Ctrl Pts',(127.249517177787,4.88610866230272,335.577888420526));
#54270=CARTESIAN_POINT('Ctrl Pts',(127.241768487229,4.89841893384281,335.441219912368));
#54271=CARTESIAN_POINT('Ctrl Pts',(127.234021408851,4.9107266441281,335.304579839235));
#54272=CARTESIAN_POINT('Ctrl Pts',(127.226274330473,4.91731584074766,335.167389738777));
#54273=CARTESIAN_POINT('Ctrl Pts',(127.218527252096,4.91815749400375,335.03016499088));
#54274=CARTESIAN_POINT('Ctrl Pts',(127.21078010879,4.9189991543137,334.892939092907));
#54275=CARTESIAN_POINT('Ctrl Pts',(127.203032965484,4.91409317278428,334.755678937783));
#54276=CARTESIAN_POINT('Ctrl Pts',(127.195285822178,4.90346265494926,334.618900204647));
#54277=CARTESIAN_POINT('Ctrl Pts',(127.18753693715,4.89282974714812,334.482090720748));
#54278=CARTESIAN_POINT('Ctrl Pts',(127.179788052122,4.87646977234223,334.345763263832));
#54279=CARTESIAN_POINT('Ctrl Pts',(127.172039167094,4.8544577024734,334.210428294962));
#54280=CARTESIAN_POINT('Ctrl Pts',(127.164282057319,4.83242226876619,334.074949680158));
#54281=CARTESIAN_POINT('Ctrl Pts',(127.156524947544,4.80472281889676,333.940466044152));
#54282=CARTESIAN_POINT('Ctrl Pts',(127.14876783777,4.77148557395651,333.80747810082));
#54283=CARTESIAN_POINT('Ctrl Pts',(127.141006582843,4.73823056809527,333.674419092983));
#54284=CARTESIAN_POINT('Ctrl Pts',(127.133245327917,4.69943198115799,333.542857745119));
#54285=CARTESIAN_POINT('Ctrl Pts',(127.125484072991,4.65526563207258,333.413278550802));
#54286=CARTESIAN_POINT('Ctrl Pts',(127.117710402586,4.61102863122245,333.283492072005));
#54287=CARTESIAN_POINT('Ctrl Pts',(127.109936732182,4.56140685106839,333.155694447515));
#54288=CARTESIAN_POINT('Ctrl Pts',(127.102163061777,4.50662422418817,333.030349989348));
#54289=CARTESIAN_POINT('Ctrl Pts',(127.0947512576,4.45439174176941,332.910840345866));
#54290=CARTESIAN_POINT('Ctrl Pts',(127.087339453423,4.39746820033474,332.793560877603));
#54291=CARTESIAN_POINT('Ctrl Pts',(127.079927649246,4.3360852037804,332.678890746204));
#54292=CARTESIAN_POINT('Ctrl Pts',(127.072152570468,4.27169364371413,332.558600290081));
#54293=CARTESIAN_POINT('Ctrl Pts',(127.064377491689,4.20219094379099,332.440801280973));
#54294=CARTESIAN_POINT('Ctrl Pts',(127.056602412911,4.12779419543709,332.32595846281));
#54295=CARTESIAN_POINT('Ctrl Pts',(127.048836901862,4.05348899701846,332.211256966047));
#54296=CARTESIAN_POINT('Ctrl Pts',(127.041071390813,3.97430194358009,332.099504747005));
#54297=CARTESIAN_POINT('Ctrl Pts',(127.033305879764,3.89049653856631,331.991143116414));
#54298=CARTESIAN_POINT('Ctrl Pts',(127.025548068241,3.80677422685534,331.882888926695));
#54299=CARTESIAN_POINT('Ctrl Pts',(127.017790256719,3.7184429138411,331.778018942502));
#54300=CARTESIAN_POINT('Ctrl Pts',(127.010032445197,3.62580982728122,331.676946260006));
#54301=CARTESIAN_POINT('Ctrl Pts',(127.002280471674,3.53324645005668,331.575949637908));
#54302=CARTESIAN_POINT('Ctrl Pts',(126.994528498151,3.43638800585055,331.478744916613));
#54303=CARTESIAN_POINT('Ctrl Pts',(126.986776524628,3.33558226070226,331.385712512183));
#54304=CARTESIAN_POINT('Ctrl Pts',(126.97902783407,3.234819206847,331.292719507032));
#54305=CARTESIAN_POINT('Ctrl Pts',(126.971279143513,3.13011246355691,331.20389556889));
#54306=CARTESIAN_POINT('Ctrl Pts',(126.963530452955,3.02184679364613,331.119584427122));
#54307=CARTESIAN_POINT('Ctrl Pts',(126.955783374577,2.91360364931215,331.035290826992));
#54308=CARTESIAN_POINT('Ctrl Pts',(126.948036296199,2.80180335939311,330.955508395656));
#54309=CARTESIAN_POINT('Ctrl Pts',(126.940289217822,2.68686360819564,330.880540446435));
#54310=CARTESIAN_POINT('Ctrl Pts',(126.932542074516,2.57192289369231,330.805571868911));
#54311=CARTESIAN_POINT('Ctrl Pts',(126.92479493121,2.45384299282088,330.73541806752));
#54312=CARTESIAN_POINT('Ctrl Pts',(126.917047787904,2.33307005490071,330.670338675898));
#54313=CARTESIAN_POINT('Ctrl Pts',(126.909298902876,2.21226996466015,330.605244653047));
#54314=CARTESIAN_POINT('Ctrl Pts',(126.901550017848,2.08877597661861,330.545227495481));
#54315=CARTESIAN_POINT('Ctrl Pts',(126.89380113282,1.96305791999246,330.490500397466));
#54316=CARTESIAN_POINT('Ctrl Pts',(126.886044023045,1.83720642492219,330.435715211544));
#54317=CARTESIAN_POINT('Ctrl Pts',(126.87828691327,1.70912650460396,330.386231457769));
#54318=CARTESIAN_POINT('Ctrl Pts',(126.870529803496,1.57930752549295,330.342213959141));
#54319=CARTESIAN_POINT('Ctrl Pts',(126.86276854857,1.44941917527031,330.298172938969));
#54320=CARTESIAN_POINT('Ctrl Pts',(126.855007293643,1.3177902894592,330.259604104139));
#54321=CARTESIAN_POINT('Ctrl Pts',(126.847246038717,1.18492343475327,330.226621792035));
#54322=CARTESIAN_POINT('Ctrl Pts',(126.839472368313,1.05184403638106,330.193586718981));
#54323=CARTESIAN_POINT('Ctrl Pts',(126.831698697908,0.917523094966202,330.166156104909));
#54324=CARTESIAN_POINT('Ctrl Pts',(126.823925027503,0.782472243155901,330.144392906012));
#54325=CARTESIAN_POINT('Ctrl Pts',(126.816513223326,0.653708040988915,330.123642789258));
#54326=CARTESIAN_POINT('Ctrl Pts',(126.809101419149,0.524280639535785,330.108044359889));
#54327=CARTESIAN_POINT('Ctrl Pts',(126.801689614972,0.394634218071375,330.09760804337));
#54328=CARTESIAN_POINT('Ctrl Pts',(126.793914536194,0.258633439293941,330.08666021189));
#54329=CARTESIAN_POINT('Ctrl Pts',(126.786139457415,0.121961840411086,330.081358711897));
#54330=CARTESIAN_POINT('Ctrl Pts',(126.778364378637,-0.0148722848646814,
330.081772486185));
#54331=CARTESIAN_POINT('Ctrl Pts',(126.770598867588,-0.151538027038381,
330.082185751298));
#54332=CARTESIAN_POINT('Ctrl Pts',(126.762833356539,-0.288365510528269,
330.088300295852));
#54333=CARTESIAN_POINT('Ctrl Pts',(126.75506784549,-0.424841030892516,330.100133352736));
#54334=CARTESIAN_POINT('Ctrl Pts',(126.747310033968,-0.561181235380335,
330.11195467711));
#54335=CARTESIAN_POINT('Ctrl Pts',(126.739552222445,-0.697169784312663,
330.129483196804));
#54336=CARTESIAN_POINT('Ctrl Pts',(126.731794410923,-0.832293037737173,
330.152684107484));
#54337=CARTESIAN_POINT('Ctrl Pts',(126.7240424374,-0.967314606629349,330.175867558744));
#54338=CARTESIAN_POINT('Ctrl Pts',(126.716290463877,-1.10147179243474,330.204714838563));
#54339=CARTESIAN_POINT('Ctrl Pts',(126.708538490354,-1.23425649901202,330.239139368019));
#54340=CARTESIAN_POINT('Ctrl Pts',(126.700789799796,-1.36698497118668,330.273549318666));
#54341=CARTESIAN_POINT('Ctrl Pts',(126.693041109239,-1.49834174261167,330.313531723274));
#54342=CARTESIAN_POINT('Ctrl Pts',(126.685292418681,-1.62782954669492,330.358949038267));
#54343=CARTESIAN_POINT('Ctrl Pts',(126.677545340303,-1.75729040975898,330.404356903807));
#54344=CARTESIAN_POINT('Ctrl Pts',(126.669798261926,-1.8848827103274,330.455197301244));
#54345=CARTESIAN_POINT('Ctrl Pts',(126.662051183548,-2.01012535281237,330.511283131174));
#54346=CARTESIAN_POINT('Ctrl Pts',(126.654304040242,-2.13536904495128,330.567369431158));
#54347=CARTESIAN_POINT('Ctrl Pts',(126.646556896936,-2.25826268299133,330.628701091568));
#54348=CARTESIAN_POINT('Ctrl Pts',(126.63880975363,-2.37834649847276,330.695043438581));
#54349=CARTESIAN_POINT('Ctrl Pts',(126.631060868602,-2.49845731134499,330.761400700762));
#54350=CARTESIAN_POINT('Ctrl Pts',(126.623311983574,-2.61575670256436,330.832770702192));
#54351=CARTESIAN_POINT('Ctrl Pts',(126.615563098546,-2.72981114097713,330.90887372511));
#54352=CARTESIAN_POINT('Ctrl Pts',(126.607805988771,-2.84398663794966,330.985057524563));
#54353=CARTESIAN_POINT('Ctrl Pts',(126.600048878997,-2.95490997629735,331.065984163479));
#54354=CARTESIAN_POINT('Ctrl Pts',(126.592291769222,-3.06217772857411,331.151331318349));
#54355=CARTESIAN_POINT('Ctrl Pts',(126.584530514296,-3.16950280130805,331.236724080009));
#54356=CARTESIAN_POINT('Ctrl Pts',(126.576769259369,-3.27316810032359,331.326541808661));
#54357=CARTESIAN_POINT('Ctrl Pts',(126.569008004443,-3.37280550919827,331.42042375977));
#54358=CARTESIAN_POINT('Ctrl Pts',(126.561234334039,-3.47260230545519,331.514455891404));
#54359=CARTESIAN_POINT('Ctrl Pts',(126.553460663634,-3.5683580627684,331.612564957409));
#54360=CARTESIAN_POINT('Ctrl Pts',(126.545686993229,-3.65974296614989,331.714354784184));
#54361=CARTESIAN_POINT('Ctrl Pts',(126.538275189052,-3.74687388029247,331.811406270033));
#54362=CARTESIAN_POINT('Ctrl Pts',(126.530863384875,-3.83003152579536,331.911803327957));
#54363=CARTESIAN_POINT('Ctrl Pts',(126.523451580698,-3.90896676476953,332.015178079947));
#54364=CARTESIAN_POINT('Ctrl Pts',(126.515660696377,-3.99193918295398,332.123839981315));
#54365=CARTESIAN_POINT('Ctrl Pts',(126.507869812057,-4.07051127335644,332.236139666177));
#54366=CARTESIAN_POINT('Ctrl Pts',(126.500078927736,-4.1443478090152,332.351686517723));
#54367=CARTESIAN_POINT('Ctrl Pts',(126.492297552703,-4.21809422231923,332.467092336726));
#54368=CARTESIAN_POINT('Ctrl Pts',(126.484516177669,-4.28711637205158,332.585737114575));
#54369=CARTESIAN_POINT('Ctrl Pts',(126.476734802636,-4.35111936196286,332.707197487691));
#54370=CARTESIAN_POINT('Ctrl Pts',(126.468961266412,-4.4150578764814,332.828535503941));
#54371=CARTESIAN_POINT('Ctrl Pts',(126.461187730187,-4.47398711153813,332.952683131024));
#54372=CARTESIAN_POINT('Ctrl Pts',(126.453414193963,-4.52765577805612,333.079188656339));
#54373=CARTESIAN_POINT('Ctrl Pts',(126.445646831812,-4.58128181862964,333.205593705569));
#54374=CARTESIAN_POINT('Ctrl Pts',(126.437879469662,-4.62965545476653,333.334352570164));
#54375=CARTESIAN_POINT('Ctrl Pts',(126.430112107512,-4.67257178717879,333.464989916593));
#54376=CARTESIAN_POINT('Ctrl Pts',(126.422349084645,-4.71546414412489,333.595554281686));
#54377=CARTESIAN_POINT('Ctrl Pts',(126.414586061778,-4.75290514467762,333.727994671824));
#54378=CARTESIAN_POINT('Ctrl Pts',(126.406823038911,-4.78473852488,333.86181710124));
#54379=CARTESIAN_POINT('Ctrl Pts',(126.399062681011,-4.81656097700833,333.995593590784));
#54380=CARTESIAN_POINT('Ctrl Pts',(126.39130232311,-4.84277955234705,334.130750797493));
#54381=CARTESIAN_POINT('Ctrl Pts',(126.38354196521,-4.86328833123651,334.266781294729));
#54382=CARTESIAN_POINT('Ctrl Pts',(126.375780911624,-4.88379894865548,334.402823986553));
#54383=CARTESIAN_POINT('Ctrl Pts',(126.368019858039,-4.89859868215799,334.539739742315));
#54384=CARTESIAN_POINT('Ctrl Pts',(126.360258804454,-4.9076330630066,334.677012722566));
#54385=CARTESIAN_POINT('Ctrl Pts',(126.354111661805,-4.91478874453972,334.785739789338));
#54386=CARTESIAN_POINT('Ctrl Pts',(126.347964519157,-4.91832857672598,334.894690727873));
#54387=CARTESIAN_POINT('Ctrl Pts',(126.341817376508,-4.91824867662815,335.003607955855));
#54388=CARTESIAN_POINT('',(124.59181841765,-4.92215355118558,335.001694350306));
#54389=CARTESIAN_POINT('Ctrl Pts',(126.341815268991,-4.91310111576097,335.003641482346));
#54390=CARTESIAN_POINT('Ctrl Pts',(126.309614694802,-4.91695460512051,335.573588454469));
#54391=CARTESIAN_POINT('Ctrl Pts',(126.184668109188,-4.56166528194609,337.7804684251));
#54392=CARTESIAN_POINT('Ctrl Pts',(125.96697551215,-1.29737390949771,340.669327103404));
#54393=CARTESIAN_POINT('Ctrl Pts',(125.688737477876,4.06537464531311,339.158987600327));
#54394=CARTESIAN_POINT('Ctrl Pts',(125.410499443602,5.69738889295149,333.832006562988));
#54395=CARTESIAN_POINT('Ctrl Pts',(125.132261409328,2.1009934468505,329.576875863238));
#54396=CARTESIAN_POINT('Ctrl Pts',(124.859368043239,-3.31733371268366,330.284605127136));
#54397=CARTESIAN_POINT('Ctrl Pts',(124.679220688574,-4.91870118483923,333.46478909301));
#54398=CARTESIAN_POINT('Ctrl Pts',(124.591819345333,-4.92563197232975,335.001679248013));
#54399=CARTESIAN_POINT('',(122.841817376472,-4.91824791957163,334.995476270419));
#54400=CARTESIAN_POINT('Ctrl Pts',(124.591817376508,-4.91824970227757,335.001711299682));
#54401=CARTESIAN_POINT('Ctrl Pts',(124.586473364599,-4.91821705436066,335.095540924806));
#54402=CARTESIAN_POINT('Ctrl Pts',(124.58112935269,-4.91549949813635,335.189320593499));
#54403=CARTESIAN_POINT('Ctrl Pts',(124.57578534078,-4.91010442639044,335.282944490035));
#54404=CARTESIAN_POINT('Ctrl Pts',(124.568010262002,-4.90225505993097,335.419159225979));
#54405=CARTESIAN_POINT('Ctrl Pts',(124.560235183224,-4.8887207487364,335.555262327574));
#54406=CARTESIAN_POINT('Ctrl Pts',(124.552460104445,-4.8695030692698,335.690740849286));
#54407=CARTESIAN_POINT('Ctrl Pts',(124.544694593396,-4.85030903838123,335.826052656051));
#54408=CARTESIAN_POINT('Ctrl Pts',(124.536929082347,-4.82544560914213,335.960741028896));
#54409=CARTESIAN_POINT('Ctrl Pts',(124.529163571298,-4.79496632083138,336.094294770431));
#54410=CARTESIAN_POINT('Ctrl Pts',(124.521405759776,-4.76451725282374,336.227716093042));
#54411=CARTESIAN_POINT('Ctrl Pts',(124.513647948254,-4.72846349306716,336.360004644515));
#54412=CARTESIAN_POINT('Ctrl Pts',(124.505890136731,-4.68691011530145,336.490656443848));
#54413=CARTESIAN_POINT('Ctrl Pts',(124.498138163208,-4.64538800777035,336.621209923558));
#54414=CARTESIAN_POINT('Ctrl Pts',(124.490386189685,-4.59837463797649,336.750128731792));
#54415=CARTESIAN_POINT('Ctrl Pts',(124.482634216162,-4.54602560084518,336.876921495151));
#54416=CARTESIAN_POINT('Ctrl Pts',(124.474885525605,-4.49369873356204,337.0036605617));
#54417=CARTESIAN_POINT('Ctrl Pts',(124.467136835047,-4.43604084209907,337.128275013629));
#54418=CARTESIAN_POINT('Ctrl Pts',(124.45938814449,-4.37325651379635,337.250291209386));
#54419=CARTESIAN_POINT('Ctrl Pts',(124.451641066112,-4.31048524829749,337.372282018654));
#54420=CARTESIAN_POINT('Ctrl Pts',(124.443893987734,-4.24258984622571,337.491675299677));
#54421=CARTESIAN_POINT('Ctrl Pts',(124.436146909356,-4.16982175769608,337.608020239865));
#54422=CARTESIAN_POINT('Ctrl Pts',(124.42839976605,-4.09705305929994,337.724366155135));
#54423=CARTESIAN_POINT('Ctrl Pts',(124.420652622744,-4.01941180026238,337.837663347221));
#54424=CARTESIAN_POINT('Ctrl Pts',(124.412905479439,-3.93719362216656,337.947488667335));
#54425=CARTESIAN_POINT('Ctrl Pts',(124.40515659441,-3.85495695967874,338.057338678514));
#54426=CARTESIAN_POINT('Ctrl Pts',(124.397407709382,-3.76814156476404,338.163714951669));
#54427=CARTESIAN_POINT('Ctrl Pts',(124.389658824354,-3.67708408910537,338.266226517581));
#54428=CARTESIAN_POINT('Ctrl Pts',(124.38190171458,-3.5859299641011,338.368846890328));
#54429=CARTESIAN_POINT('Ctrl Pts',(124.374144604805,-3.49052502400119,338.467594068925));
#54430=CARTESIAN_POINT('Ctrl Pts',(124.36638749503,-3.39124398410291,338.562112758292));
#54431=CARTESIAN_POINT('Ctrl Pts',(124.358626240104,-3.2919098915913,338.656681955424));
#54432=CARTESIAN_POINT('Ctrl Pts',(124.350864985178,-3.18869586608189,338.74701790363));
#54433=CARTESIAN_POINT('Ctrl Pts',(124.343103730252,-3.08200982573676,338.83280556467));
#54434=CARTESIAN_POINT('Ctrl Pts',(124.335330059847,-2.97515312249605,338.918730458009));
#54435=CARTESIAN_POINT('Ctrl Pts',(124.327556389442,-2.86481362045928,339.000092292927));
#54436=CARTESIAN_POINT('Ctrl Pts',(124.319782719038,-2.7514290660605,339.07661883881));
#54437=CARTESIAN_POINT('Ctrl Pts',(124.312370914861,-2.64332258994761,339.14958305557));
#54438=CARTESIAN_POINT('Ctrl Pts',(124.304959110683,-2.53244842075332,339.218151866638));
#54439=CARTESIAN_POINT('Ctrl Pts',(124.297547306506,-2.41920518882687,339.282129063545));
#54440=CARTESIAN_POINT('Ctrl Pts',(124.289772227728,-2.30041156876948,339.349241973449));
#54441=CARTESIAN_POINT('Ctrl Pts',(124.28199714895,-2.17863537461952,339.411513880292));
#54442=CARTESIAN_POINT('Ctrl Pts',(124.274222070171,-2.05430880633529,339.468668525491));
#54443=CARTESIAN_POINT('Ctrl Pts',(124.266456559122,-1.93013522980844,339.525752838261));
#54444=CARTESIAN_POINT('Ctrl Pts',(124.258691048073,-1.80341787540803,339.577732257139));
#54445=CARTESIAN_POINT('Ctrl Pts',(124.250925537024,-1.67461559310128,339.624375166208));
#54446=CARTESIAN_POINT('Ctrl Pts',(124.243167725502,-1.54594101863225,339.670971828697));
#54447=CARTESIAN_POINT('Ctrl Pts',(124.23540991398,-1.41518599527714,339.712242378862));
#54448=CARTESIAN_POINT('Ctrl Pts',(124.227652102457,-1.28283119284316,339.748002442414));
#54449=CARTESIAN_POINT('Ctrl Pts',(124.219900128934,-1.1505759915954,339.783735595384));
#54450=CARTESIAN_POINT('Ctrl Pts',(124.212148155411,-1.01672378336661,339.813966414233));
#54451=CARTESIAN_POINT('Ctrl Pts',(124.204396181888,-0.881771975873617,
339.838559831713));
#54452=CARTESIAN_POINT('Ctrl Pts',(124.196647491331,-0.746877320551128,
339.863142833865));
#54453=CARTESIAN_POINT('Ctrl Pts',(124.188898800773,-0.610884375911698,
339.882093113171));
#54454=CARTESIAN_POINT('Ctrl Pts',(124.181150110216,-0.474302151189679,
339.895326396868));
#54455=CARTESIAN_POINT('Ctrl Pts',(124.173403031838,-0.337748343540318,
339.90855692727));
#54456=CARTESIAN_POINT('Ctrl Pts',(124.16565595346,-0.200605888485871,339.91607279033));
#54457=CARTESIAN_POINT('Ctrl Pts',(124.157908875082,-0.0633899580356592,
339.917841475253));
#54458=CARTESIAN_POINT('Ctrl Pts',(124.150161731776,0.0738271224160726,
339.919610175));
#54459=CARTESIAN_POINT('Ctrl Pts',(124.142414588471,0.211117288649995,339.9156315955));
#54460=CARTESIAN_POINT('Ctrl Pts',(124.134667445165,0.34796471720093,339.905925357981));
#54461=CARTESIAN_POINT('Ctrl Pts',(124.126918560137,0.484842911959203,339.896216938294));
#54462=CARTESIAN_POINT('Ctrl Pts',(124.119169675109,0.621277781148712,339.880778325859));
#54463=CARTESIAN_POINT('Ctrl Pts',(124.111420790081,0.756758368867927,339.859681042378));
#54464=CARTESIAN_POINT('Ctrl Pts',(124.103663680306,0.892382757082815,339.838561366023));
#54465=CARTESIAN_POINT('Ctrl Pts',(124.095906570531,1.02705045366658,339.811771080969));
#54466=CARTESIAN_POINT('Ctrl Pts',(124.088149460756,1.16025990345685,339.779433022748));
#54467=CARTESIAN_POINT('Ctrl Pts',(124.08038820583,1.29354053611778,339.747077684102));
#54468=CARTESIAN_POINT('Ctrl Pts',(124.072626950904,1.42536099381965,339.709168773126));
#54469=CARTESIAN_POINT('Ctrl Pts',(124.064865695978,1.55523560626181,339.665878831637));
#54470=CARTESIAN_POINT('Ctrl Pts',(124.057092025573,1.68531797575783,339.622519640349));
#54471=CARTESIAN_POINT('Ctrl Pts',(124.049318355169,1.81344791435055,339.573762356511));
#54472=CARTESIAN_POINT('Ctrl Pts',(124.041544684764,1.93915960779533,339.519827770833));
#54473=CARTESIAN_POINT('Ctrl Pts',(124.034132880587,2.05901939166561,339.468403853095));
#54474=CARTESIAN_POINT('Ctrl Pts',(124.02672107641,2.17668074265337,339.412273916969));
#54475=CARTESIAN_POINT('Ctrl Pts',(124.019309272233,2.29176294311589,339.35166699956));
#54476=CARTESIAN_POINT('Ctrl Pts',(124.011534193454,2.41248566503534,339.288089556591));
#54477=CARTESIAN_POINT('Ctrl Pts',(124.003759114676,2.5307515261828,339.219384258902));
#54478=CARTESIAN_POINT('Ctrl Pts',(123.995984035898,2.64609432662721,339.145765053291));
#54479=CARTESIAN_POINT('Ctrl Pts',(123.988218524849,2.76129519041259,339.0722364408));
#54480=CARTESIAN_POINT('Ctrl Pts',(123.980453013799,2.87357982418608,338.993806160222));
#54481=CARTESIAN_POINT('Ctrl Pts',(123.97268750275,2.98250514713447,338.91073472762));
#54482=CARTESIAN_POINT('Ctrl Pts',(123.964929691228,3.09132247030802,338.827745660586));
#54483=CARTESIAN_POINT('Ctrl Pts',(123.957171879706,3.19678680226941,338.740124834709));
#54484=CARTESIAN_POINT('Ctrl Pts',(123.949414068184,3.29848298073142,338.648176679977));
#54485=CARTESIAN_POINT('Ctrl Pts',(123.941662094661,3.40010262959414,338.556297719146));
#54486=CARTESIAN_POINT('Ctrl Pts',(123.933910121138,3.49795948042143,338.460098172359));
#54487=CARTESIAN_POINT('Ctrl Pts',(123.926158147615,3.59167077642494,338.359923227735));
#54488=CARTESIAN_POINT('Ctrl Pts',(123.918409457057,3.68534238563896,338.259790707261));
#54489=CARTESIAN_POINT('Ctrl Pts',(123.9106607665,3.77487166541158,338.15568642233));
#54490=CARTESIAN_POINT('Ctrl Pts',(123.902912075942,3.8599122948756,338.047992804842));
#54491=CARTESIAN_POINT('Ctrl Pts',(123.895164997564,3.94493523092639,337.94032159391));
#54492=CARTESIAN_POINT('Ctrl Pts',(123.887417919186,4.02547113217919,337.82906284241));
#54493=CARTESIAN_POINT('Ctrl Pts',(123.879670840809,4.10121387047949,337.714632176021));
#54494=CARTESIAN_POINT('Ctrl Pts',(123.871923697503,4.17695724357684,337.600200550592));
#54495=CARTESIAN_POINT('Ctrl Pts',(123.864176554197,4.24790715785358,337.48259728319));
#54496=CARTESIAN_POINT('Ctrl Pts',(123.856429410891,4.31380097154295,337.362266758945));
#54497=CARTESIAN_POINT('Ctrl Pts',(123.848680525863,4.37970959956056,337.241909181843));
#54498=CARTESIAN_POINT('Ctrl Pts',(123.840931640835,4.44055967734475,337.118823470575));
#54499=CARTESIAN_POINT('Ctrl Pts',(123.833182755807,4.49613484146449,336.993478003357));
#54500=CARTESIAN_POINT('Ctrl Pts',(123.825425646032,4.55176899363768,336.867999493165));
#54501=CARTESIAN_POINT('Ctrl Pts',(123.817668536257,4.60211688924213,336.74025679363));
#54502=CARTESIAN_POINT('Ctrl Pts',(123.809911426483,4.64701040301992,336.610738146542));
#54503=CARTESIAN_POINT('Ctrl Pts',(123.802150171557,4.69192790645605,336.48115028883));
#54504=CARTESIAN_POINT('Ctrl Pts',(123.79438891663,4.73138510798403,336.34978496674));
#54505=CARTESIAN_POINT('Ctrl Pts',(123.786627661704,4.76526427763109,336.217143963068));
#54506=CARTESIAN_POINT('Ctrl Pts',(123.7788539913,4.79919764290838,336.084290777018));
#54507=CARTESIAN_POINT('Ctrl Pts',(123.771080320895,4.82753506460514,335.950158214146));
#54508=CARTESIAN_POINT('Ctrl Pts',(123.76330665049,4.85021013152304,335.815257470111));
#54509=CARTESIAN_POINT('Ctrl Pts',(123.755894846313,4.87182966862059,335.686636388166));
#54510=CARTESIAN_POINT('Ctrl Pts',(123.748483042136,4.88830211627918,335.557317318753));
#54511=CARTESIAN_POINT('Ctrl Pts',(123.741071237959,4.89961404852394,335.427744360579));
#54512=CARTESIAN_POINT('Ctrl Pts',(123.733296159181,4.91148041226454,335.291820645746));
#54513=CARTESIAN_POINT('Ctrl Pts',(123.725521080402,4.91770510523584,335.155187981128));
#54514=CARTESIAN_POINT('Ctrl Pts',(123.717746001624,4.91821575232965,335.018354183078));
#54515=CARTESIAN_POINT('Ctrl Pts',(123.709980490575,4.91872577103971,334.881688767728));
#54516=CARTESIAN_POINT('Ctrl Pts',(123.702214979526,4.91353573309087,334.744823098551));
#54517=CARTESIAN_POINT('Ctrl Pts',(123.694449468477,4.90262493554631,334.608270751846));
#54518=CARTESIAN_POINT('Ctrl Pts',(123.686691656954,4.89172495608928,334.47185379719));
#54519=CARTESIAN_POINT('Ctrl Pts',(123.678933845432,4.87511553586719,334.335749933896));
#54520=CARTESIAN_POINT('Ctrl Pts',(123.67117603391,4.852828008416,334.200473025325));
#54521=CARTESIAN_POINT('Ctrl Pts',(123.663424060387,4.830557253036,334.065297916917));
#54522=CARTESIAN_POINT('Ctrl Pts',(123.655672086864,4.80261695882242,333.930948908676));
#54523=CARTESIAN_POINT('Ctrl Pts',(123.647920113341,4.76909027017057,333.797934670051));
#54524=CARTESIAN_POINT('Ctrl Pts',(123.640171422783,4.73557778009128,333.664976763035));
#54525=CARTESIAN_POINT('Ctrl Pts',(123.632422732226,4.69648369639993,333.533352879573));
#54526=CARTESIAN_POINT('Ctrl Pts',(123.624674041668,4.65194220014464,333.403561204113));
#54527=CARTESIAN_POINT('Ctrl Pts',(123.61692696329,4.60740997111966,333.273796532895));
#54528=CARTESIAN_POINT('Ctrl Pts',(123.609179884912,4.55743271069921,333.145863680911));
#54529=CARTESIAN_POINT('Ctrl Pts',(123.601432806535,4.50219426387252,333.02024499676));
#54530=CARTESIAN_POINT('Ctrl Pts',(123.593685663229,4.44695535409447,332.894625259804));
#54531=CARTESIAN_POINT('Ctrl Pts',(123.585938519923,4.38645532730135,332.771320087173));
#54532=CARTESIAN_POINT('Ctrl Pts',(123.578191376617,4.32092574589757,332.650790822226));
#54533=CARTESIAN_POINT('Ctrl Pts',(123.570442491589,4.25538143205276,332.53023445974));
#54534=CARTESIAN_POINT('Ctrl Pts',(123.562693606561,4.184805500195,332.412455590129));
#54535=CARTESIAN_POINT('Ctrl Pts',(123.554944721533,4.1094747328909,332.297889624343));
#54536=CARTESIAN_POINT('Ctrl Pts',(123.547187611758,4.03406400873195,332.183202057058));
#54537=CARTESIAN_POINT('Ctrl Pts',(123.539430501983,3.95388858269473,332.071734532926));
#54538=CARTESIAN_POINT('Ctrl Pts',(123.531673392209,3.86926804549347,331.963892647711));
#54539=CARTESIAN_POINT('Ctrl Pts',(123.523912137283,3.78460228978281,331.855993135241));
#54540=CARTESIAN_POINT('Ctrl Pts',(123.516150882356,3.69548694368209,331.75172341917));
#54541=CARTESIAN_POINT('Ctrl Pts',(123.50838962743,3.60228025660474,331.651454044607));
#54542=CARTESIAN_POINT('Ctrl Pts',(123.500615957026,3.50892446920409,331.551024271723));
#54543=CARTESIAN_POINT('Ctrl Pts',(123.492842286621,3.41146454037353,331.454607902971));
#54544=CARTESIAN_POINT('Ctrl Pts',(123.485068616216,3.31029440653752,331.362537422248));
#54545=CARTESIAN_POINT('Ctrl Pts',(123.477656812039,3.21383376677184,331.274752844554));
#54546=CARTESIAN_POINT('Ctrl Pts',(123.470245007862,3.11400078901798,331.190918843107));
#54547=CARTESIAN_POINT('Ctrl Pts',(123.462833203685,3.0111616597879,331.11128703539));
#54548=CARTESIAN_POINT('Ctrl Pts',(123.455058124907,2.90328207849218,331.027752235566));
#54549=CARTESIAN_POINT('Ctrl Pts',(123.447283046128,2.79175329442391,330.948577983643));
#54550=CARTESIAN_POINT('Ctrl Pts',(123.43950796735,2.67696317486632,330.874099949961));
#54551=CARTESIAN_POINT('Ctrl Pts',(123.431742456301,2.56231431185874,330.799713566242));
#54552=CARTESIAN_POINT('Ctrl Pts',(123.423976945252,2.44441242340842,330.730012112935));
#54553=CARTESIAN_POINT('Ctrl Pts',(123.416211434203,2.3236781832345,330.665290925188));
#54554=CARTESIAN_POINT('Ctrl Pts',(123.40845362268,2.20306365141118,330.600633908686));
#54555=CARTESIAN_POINT('Ctrl Pts',(123.400695811158,2.07962269878878,330.540947514431));
#54556=CARTESIAN_POINT('Ctrl Pts',(123.392937999636,1.95380440040298,330.486483474333));
#54557=CARTESIAN_POINT('Ctrl Pts',(123.385186026113,1.82808078427677,330.432060420153));
#54558=CARTESIAN_POINT('Ctrl Pts',(123.37743405259,1.69998374062414,330.382852052333));
#54559=CARTESIAN_POINT('Ctrl Pts',(123.369682079067,1.56998601463972,330.339063723206));
#54560=CARTESIAN_POINT('Ctrl Pts',(123.361933388509,1.44004334276939,330.295293938462));
#54561=CARTESIAN_POINT('Ctrl Pts',(123.354184697952,1.30820195918995,330.256939751555));
#54562=CARTESIAN_POINT('Ctrl Pts',(123.346436007394,1.17495341089747,330.224157922971));
#54563=CARTESIAN_POINT('Ctrl Pts',(123.338688929016,1.04173258607837,330.19138291492));
#54564=CARTESIAN_POINT('Ctrl Pts',(123.330941850639,0.907105558209408,330.164178052432));
#54565=CARTESIAN_POINT('Ctrl Pts',(123.323194772261,0.771577433590507,330.142649762836));
#54566=CARTESIAN_POINT('Ctrl Pts',(123.315447628955,0.636048173115384,330.121121292813));
#54567=CARTESIAN_POINT('Ctrl Pts',(123.307700485649,0.4996181868615,330.105269551895));
#54568=CARTESIAN_POINT('Ctrl Pts',(123.299953342343,0.362800740003776,330.095149473679));
#54569=CARTESIAN_POINT('Ctrl Pts',(123.292204457315,0.225952533679329,330.085027120254));
#54570=CARTESIAN_POINT('Ctrl Pts',(123.284455572287,0.0887170831463317,
330.080639022528));
#54571=CARTESIAN_POINT('Ctrl Pts',(123.276706687259,-0.0483896823070491,
330.081988053985));
#54572=CARTESIAN_POINT('Ctrl Pts',(123.268949577484,-0.18564197429786,330.083338517318));
#54573=CARTESIAN_POINT('Ctrl Pts',(123.26119246771,-0.322764916889646,330.090438270227));
#54574=CARTESIAN_POINT('Ctrl Pts',(123.253435357935,-0.459244487077345,
330.103238053204));
#54575=CARTESIAN_POINT('Ctrl Pts',(123.245674103009,-0.595796987583629,
330.116044675976));
#54576=CARTESIAN_POINT('Ctrl Pts',(123.237912848082,-0.731705043536764,
330.134557345343));
#54577=CARTESIAN_POINT('Ctrl Pts',(123.230151593156,-0.86646318633607,330.158675324952));
#54578=CARTESIAN_POINT('Ctrl Pts',(123.222377922752,-1.00143689824623,330.182831885469));
#54579=CARTESIAN_POINT('Ctrl Pts',(123.214604252347,-1.13525663942247,330.212611589337));
#54580=CARTESIAN_POINT('Ctrl Pts',(123.206830581942,-1.26742963545979,330.247863093128));
#54581=CARTESIAN_POINT('Ctrl Pts',(123.199418777765,-1.39344994673317,330.281473630936));
#54582=CARTESIAN_POINT('Ctrl Pts',(123.192006973588,-1.5179730997478,330.320057923196));
#54583=CARTESIAN_POINT('Ctrl Pts',(123.184595169411,-1.64058933946203,330.363444200514));
#54584=CARTESIAN_POINT('Ctrl Pts',(123.176820090632,-1.76921536633913,330.408956968525));
#54585=CARTESIAN_POINT('Ctrl Pts',(123.169045011854,-1.89614930846979,330.459898171677));
#54586=CARTESIAN_POINT('Ctrl Pts',(123.161269933076,-2.0208989962603,330.516123294579));
#54587=CARTESIAN_POINT('Ctrl Pts',(123.153504422027,-2.14549517161785,330.572279228888));
#54588=CARTESIAN_POINT('Ctrl Pts',(123.145738910978,-2.26791208776777,330.63370598636));
#54589=CARTESIAN_POINT('Ctrl Pts',(123.137973399929,-2.38767374039788,330.700209636283));
#54590=CARTESIAN_POINT('Ctrl Pts',(123.130215588406,-2.50731664900086,330.766647347644));
#54591=CARTESIAN_POINT('Ctrl Pts',(123.122457776884,-2.6243091937875,330.838151745465));
#54592=CARTESIAN_POINT('Ctrl Pts',(123.114699965362,-2.73819666775436,330.91448141955));
#54593=CARTESIAN_POINT('Ctrl Pts',(123.106947991839,-2.85199843778543,330.990753653135));
#54594=CARTESIAN_POINT('Ctrl Pts',(123.099196018316,-2.96269946462649,331.071843718571));
#54595=CARTESIAN_POINT('Ctrl Pts',(123.091444044793,-3.06987123357102,331.157465202266));
#54596=CARTESIAN_POINT('Ctrl Pts',(123.083695354235,-3.17699761520774,331.243050425213));
#54597=CARTESIAN_POINT('Ctrl Pts',(123.075946663678,-3.28059740694012,331.333163006079));
#54598=CARTESIAN_POINT('Ctrl Pts',(123.06819797312,-3.3802727812472,331.427474424604));
#54599=CARTESIAN_POINT('Ctrl Pts',(123.060450894742,-3.47992741726014,331.52176622085));
#54600=CARTESIAN_POINT('Ctrl Pts',(123.052703816364,-3.57565897619402,331.62025484862));
#54601=CARTESIAN_POINT('Ctrl Pts',(123.044956737986,-3.66710461903429,331.722573147184));
#54602=CARTESIAN_POINT('Ctrl Pts',(123.037209594681,-3.75855102827707,331.824892303275));
#54603=CARTESIAN_POINT('Ctrl Pts',(123.029462451375,-3.84571118930982,331.931040902738));
#54604=CARTESIAN_POINT('Ctrl Pts',(123.021715308069,-3.92826115006238,332.04061705766));
#54605=CARTESIAN_POINT('Ctrl Pts',(123.013966423041,-4.01082966979873,332.150217847628));
#54606=CARTESIAN_POINT('Ctrl Pts',(123.006217538013,-4.08878569164476,332.263247414303));
#54607=CARTESIAN_POINT('Ctrl Pts',(122.998468652985,-4.16184760028338,332.379273456746));
#54608=CARTESIAN_POINT('Ctrl Pts',(122.99071154321,-4.23498705758672,332.49542265043));
#54609=CARTESIAN_POINT('Ctrl Pts',(122.982954433435,-4.30322181624805,332.614574341928));
#54610=CARTESIAN_POINT('Ctrl Pts',(122.975197323661,-4.36631513229625,332.736269621183));
#54611=CARTESIAN_POINT('Ctrl Pts',(122.967436068734,-4.42944216339519,332.858029930504));
#54612=CARTESIAN_POINT('Ctrl Pts',(122.959674813808,-4.48742211225222,332.982336181877));
#54613=CARTESIAN_POINT('Ctrl Pts',(122.951913558882,-4.54006615215355,333.108708801752));
#54614=CARTESIAN_POINT('Ctrl Pts',(122.944139888478,-4.59279440536205,333.235283576634));
#54615=CARTESIAN_POINT('Ctrl Pts',(122.936366218073,-4.64016955758274,333.36393095843));
#54616=CARTESIAN_POINT('Ctrl Pts',(122.928592547668,-4.68205220822821,333.494154662017));
#54617=CARTESIAN_POINT('Ctrl Pts',(122.921180743491,-4.7219852114098,333.618316420872));
#54618=CARTESIAN_POINT('Ctrl Pts',(122.913768939314,-4.75692548012175,333.743910771334));
#54619=CARTESIAN_POINT('Ctrl Pts',(122.906357135137,-4.78679571694647,333.870500187374));
#54620=CARTESIAN_POINT('Ctrl Pts',(122.895600508699,-4.83014588803358,334.054217272555));
#54621=CARTESIAN_POINT('Ctrl Pts',(122.884843882261,-4.86293462881886,334.240514229832));
#54622=CARTESIAN_POINT('Ctrl Pts',(122.874087255823,-4.88491651648687,334.428358775582));
#54623=CARTESIAN_POINT('Ctrl Pts',(122.863330629385,-4.90689840415487,334.616203321333));
#54624=CARTESIAN_POINT('Ctrl Pts',(122.852574002947,-4.91807327065724,334.805596101312));
#54625=CARTESIAN_POINT('Ctrl Pts',(122.841817376508,-4.91824791957104,334.995476269776));
#54626=CARTESIAN_POINT('',(121.091817376452,-4.9182499653126,335.000584125506));
#54627=CARTESIAN_POINT('Ctrl Pts',(122.841817376472,-4.91824791957163,334.995476270419));
#54628=CARTESIAN_POINT('Ctrl Pts',(122.834159905798,-4.9183722493281,335.130648931646));
#54629=CARTESIAN_POINT('Ctrl Pts',(122.826502435125,-4.91291978064133,335.265979802592));
#54630=CARTESIAN_POINT('Ctrl Pts',(122.818844964452,-4.90187821147916,335.400965163482));
#54631=CARTESIAN_POINT('Ctrl Pts',(122.810898053469,-4.89041928842385,335.541052758035));
#54632=CARTESIAN_POINT('Ctrl Pts',(122.802951142486,-4.87294038696696,335.680767772425));
#54633=CARTESIAN_POINT('Ctrl Pts',(122.795004231503,-4.84948717539217,335.819546946921));
#54634=CARTESIAN_POINT('Ctrl Pts',(122.787355074242,-4.82691270538579,335.953126363205));
#54635=CARTESIAN_POINT('Ctrl Pts',(122.77970591698,-4.7988036110565,336.085838369296));
#54636=CARTESIAN_POINT('Ctrl Pts',(122.772056759719,-4.76525336520633,336.217186685718));
#54637=CARTESIAN_POINT('Ctrl Pts',(122.764408668907,-4.73170779695223,336.348516689477));
#54638=CARTESIAN_POINT('Ctrl Pts',(122.756760578096,-4.69272268492862,336.478482992305));
#54639=CARTESIAN_POINT('Ctrl Pts',(122.749112487284,-4.64844220410786,336.606601424613));
#54640=CARTESIAN_POINT('Ctrl Pts',(122.741463706305,-4.60415772739081,336.734731418403));
#54641=CARTESIAN_POINT('Ctrl Pts',(122.733814925325,-4.55457706320149,336.861012830311));
#54642=CARTESIAN_POINT('Ctrl Pts',(122.726166144346,-4.49989347265338,336.984979042023));
#54643=CARTESIAN_POINT('Ctrl Pts',(122.718514916266,-4.44519238699958,337.108984914664));
#54644=CARTESIAN_POINT('Ctrl Pts',(122.710863688186,-4.3853852907965,337.230673746815));
#54645=CARTESIAN_POINT('Ctrl Pts',(122.703212460106,-4.32071231699118,337.349601697374));
#54646=CARTESIAN_POINT('Ctrl Pts',(122.695552944593,-4.25596929260321,337.468658464835));
#54647=CARTESIAN_POINT('Ctrl Pts',(122.687893429079,-4.18635006378195,337.584948029246));
#54648=CARTESIAN_POINT('Ctrl Pts',(122.680233913565,-4.11213931729558,337.69805361282));
#54649=CARTESIAN_POINT('Ctrl Pts',(122.672569467805,-4.03788080313057,337.811231999747));
#54650=CARTESIAN_POINT('Ctrl Pts',(122.664905022045,-3.9590251217713,337.921222000921));
#54651=CARTESIAN_POINT('Ctrl Pts',(122.657240576285,-3.87589767980065,338.02763938378));
#54652=CARTESIAN_POINT('Ctrl Pts',(122.649565403942,-3.79265389890404,338.134205700417));
#54653=CARTESIAN_POINT('Ctrl Pts',(122.641890231599,-3.70512668721262,338.237189117517));
#54654=CARTESIAN_POINT('Ctrl Pts',(122.634215059256,-3.6136788986125,338.336241580015));
#54655=CARTESIAN_POINT('Ctrl Pts',(122.632183073125,-3.58946828419969,338.36246551624));
#54656=CARTESIAN_POINT('Ctrl Pts',(122.630151086994,-3.56498305269611,338.38841414331));
#54657=CARTESIAN_POINT('Ctrl Pts',(122.628119100863,-3.54023031797993,338.41408148089));
#54658=CARTESIAN_POINT('Ctrl Pts',(122.620344022085,-3.44551782980707,338.51229355462));
#54659=CARTESIAN_POINT('Ctrl Pts',(122.612568943306,-3.34656572341985,338.606716605221));
#54660=CARTESIAN_POINT('Ctrl Pts',(122.604793864528,-3.24370943285665,338.696962561035));
#54661=CARTESIAN_POINT('Ctrl Pts',(122.597028353479,-3.1409797135072,338.787097463455));
#54662=CARTESIAN_POINT('Ctrl Pts',(122.58926284243,-3.03435566025973,338.873065243246));
#54663=CARTESIAN_POINT('Ctrl Pts',(122.581497331381,-2.92421098485638,338.954513014082));
#54664=CARTESIAN_POINT('Ctrl Pts',(122.573739519859,-2.81417551821922,339.035880029216));
#54665=CARTESIAN_POINT('Ctrl Pts',(122.565981708336,-2.70062668838819,339.112735723133));
#54666=CARTESIAN_POINT('Ctrl Pts',(122.558223896814,-2.58397259673982,339.1847662637));
#54667=CARTESIAN_POINT('Ctrl Pts',(122.550471923291,-2.46740629099456,339.256742599));
#54668=CARTESIAN_POINT('Ctrl Pts',(122.542719949768,-2.3477397059761,339.323900803905));
#54669=CARTESIAN_POINT('Ctrl Pts',(122.534967976245,-2.22541105112032,339.385969529768));
#54670=CARTESIAN_POINT('Ctrl Pts',(122.527219285688,-2.10313420252278,339.448011969488));
#54671=CARTESIAN_POINT('Ctrl Pts',(122.51947059513,-1.9781978742298,339.504969040604));
#54672=CARTESIAN_POINT('Ctrl Pts',(122.511721904572,-1.85106588508885,339.556614768834));
#54673=CARTESIAN_POINT('Ctrl Pts',(122.503974826194,-1.72396034682007,339.60824975174));
#54674=CARTESIAN_POINT('Ctrl Pts',(122.496227747817,-1.59466041826794,339.654575442801));
#54675=CARTESIAN_POINT('Ctrl Pts',(122.488480669439,-1.463650590928,339.695413720874));
#54676=CARTESIAN_POINT('Ctrl Pts',(122.480733526133,-1.33263966559965,339.736252341212));
#54677=CARTESIAN_POINT('Ctrl Pts',(122.472986382827,-1.19991918606457,339.77160334051));
#54678=CARTESIAN_POINT('Ctrl Pts',(122.465239239521,-1.06598913971513,339.801338377631));
#54679=CARTESIAN_POINT('Ctrl Pts',(122.457490354493,-0.93202898304785,339.831080099819));
#54680=CARTESIAN_POINT('Ctrl Pts',(122.449741469465,-0.796859099951614,
339.855203262722));
#54681=CARTESIAN_POINT('Ctrl Pts',(122.441992584437,-0.660989617969191,
339.873630657676));
#54682=CARTESIAN_POINT('Ctrl Pts',(122.434235474662,-0.524975922714567,
339.892077611657));
#54683=CARTESIAN_POINT('Ctrl Pts',(122.426478364888,-0.388261533177497,
339.904816668529));
#54684=CARTESIAN_POINT('Ctrl Pts',(122.418721255113,-0.25136220488622,339.911822482995));
#54685=CARTESIAN_POINT('Ctrl Pts',(122.410960000187,-0.114389721971095,
339.918832041144));
#54686=CARTESIAN_POINT('Ctrl Pts',(122.40319874526,0.0227675059574034,339.920102248649));
#54687=CARTESIAN_POINT('Ctrl Pts',(122.395437490334,0.159594768660187,339.915659932534));
#54688=CARTESIAN_POINT('Ctrl Pts',(122.38766381993,0.296640910391301,339.91121051016));
#54689=CARTESIAN_POINT('Ctrl Pts',(122.379890149525,0.433355642122252,339.901030332424));
#54690=CARTESIAN_POINT('Ctrl Pts',(122.37211647912,0.569229520832275,339.885198134683));
#54691=CARTESIAN_POINT('Ctrl Pts',(122.364704674943,0.698778437799172,339.870102929556));
#54692=CARTESIAN_POINT('Ctrl Pts',(122.357292870766,0.827562739132954,339.849870110281));
#54693=CARTESIAN_POINT('Ctrl Pts',(122.349881066589,0.955152190086452,339.824610591154));
#54694=CARTESIAN_POINT('Ctrl Pts',(122.342105987811,1.08899518010035,339.79811302775));
#54695=CARTESIAN_POINT('Ctrl Pts',(122.334330909032,1.22194620041557,339.765999821112));
#54696=CARTESIAN_POINT('Ctrl Pts',(122.326555830254,1.3534973906889,339.728343037037));
#54697=CARTESIAN_POINT('Ctrl Pts',(122.318790319205,1.48488669884765,339.690732592033));
#54698=CARTESIAN_POINT('Ctrl Pts',(122.311024808156,1.61487923221551,339.647592249408));
#54699=CARTESIAN_POINT('Ctrl Pts',(122.303259297107,1.74297600428424,339.599045304298));
#54700=CARTESIAN_POINT('Ctrl Pts',(122.295501485584,1.87094576803062,339.550546493627));
#54701=CARTESIAN_POINT('Ctrl Pts',(122.287743674062,1.99702314794207,339.496651886121));
#54702=CARTESIAN_POINT('Ctrl Pts',(122.27998586254,2.12072338880957,339.43753483036));
#54703=CARTESIAN_POINT('Ctrl Pts',(122.272233889017,2.24433054132276,339.378462262058));
#54704=CARTESIAN_POINT('Ctrl Pts',(122.264481915494,2.3655637642055,339.314175235953));
#54705=CARTESIAN_POINT('Ctrl Pts',(122.256729941971,2.48395773432029,339.244895409384));
#54706=CARTESIAN_POINT('Ctrl Pts',(122.248981251413,2.6023015645186,339.175644922863));
#54707=CARTESIAN_POINT('Ctrl Pts',(122.241232560856,2.71780819683018,339.101406038379));
#54708=CARTESIAN_POINT('Ctrl Pts',(122.233483870298,2.83003660566866,339.022446503445));
#54709=CARTESIAN_POINT('Ctrl Pts',(122.22573679192,2.9422416644492,338.943503396702));
#54710=CARTESIAN_POINT('Ctrl Pts',(122.217989713542,3.05116953694549,338.85984181789));
#54711=CARTESIAN_POINT('Ctrl Pts',(122.210242635165,3.15640825113983,338.771772794673));
#54712=CARTESIAN_POINT('Ctrl Pts',(122.202495491859,3.26164784733589,338.683703033353));
#54713=CARTESIAN_POINT('Ctrl Pts',(122.194748348553,3.36319792380149,338.591226004805));
#54714=CARTESIAN_POINT('Ctrl Pts',(122.187001205247,3.4606799838699,338.494692706339));
#54715=CARTESIAN_POINT('Ctrl Pts',(122.179252320219,3.55818395997528,338.398137705139));
#54716=CARTESIAN_POINT('Ctrl Pts',(122.171503435191,3.65161782209463,338.297524894353));
#54717=CARTESIAN_POINT('Ctrl Pts',(122.163754550163,3.74064058453279,338.193241469079));
#54718=CARTESIAN_POINT('Ctrl Pts',(122.155997440388,3.8297578366506,338.0888473563));
#54719=CARTESIAN_POINT('Ctrl Pts',(122.148240330613,3.91445438219807,337.980775144105));
#54720=CARTESIAN_POINT('Ctrl Pts',(122.140483220839,3.99442980286522,337.869444826527));
#54721=CARTESIAN_POINT('Ctrl Pts',(122.132721965912,4.07444795984006,337.758055017587));
#54722=CARTESIAN_POINT('Ctrl Pts',(122.124960710986,4.14973975054163,337.643403960666));
#54723=CARTESIAN_POINT('Ctrl Pts',(122.11719945606,4.2200491951423,337.525939004228));
#54724=CARTESIAN_POINT('Ctrl Pts',(122.109425785655,4.29047111194052,337.408286142141));
#54725=CARTESIAN_POINT('Ctrl Pts',(122.101652115251,4.35589456932713,337.287810729236));
#54726=CARTESIAN_POINT('Ctrl Pts',(122.093878444846,4.41611008869309,337.164983775238));
#54727=CARTESIAN_POINT('Ctrl Pts',(122.086466640669,4.47352256114517,337.047874445499));
#54728=CARTESIAN_POINT('Ctrl Pts',(122.079054836492,4.52620092686151,336.928627839548));
#54729=CARTESIAN_POINT('Ctrl Pts',(122.071643032315,4.57400563133066,336.80766577305));
#54730=CARTESIAN_POINT('Ctrl Pts',(122.063867953537,4.62415338676901,336.680774995344));
#54731=CARTESIAN_POINT('Ctrl Pts',(122.056092874758,4.66909613202267,336.551595347209));
#54732=CARTESIAN_POINT('Ctrl Pts',(122.04831779598,4.70861963638458,336.420592898178));
#54733=CARTESIAN_POINT('Ctrl Pts',(122.040552284931,4.74809450455819,336.289751656001));
#54734=CARTESIAN_POINT('Ctrl Pts',(122.032786773882,4.78216328886125,336.157092446636));
#54735=CARTESIAN_POINT('Ctrl Pts',(122.025021262833,4.81065964057301,336.023101600557));
#54736=CARTESIAN_POINT('Ctrl Pts',(122.01726345131,4.83912773806905,335.889243606792));
#54737=CARTESIAN_POINT('Ctrl Pts',(122.009505639788,4.86203431741517,335.754056983689));
#54738=CARTESIAN_POINT('Ctrl Pts',(122.001747828266,4.87926282227019,335.618043181106));
#54739=CARTESIAN_POINT('Ctrl Pts',(121.993995854743,4.89647836212897,335.482131733224));
#54740=CARTESIAN_POINT('Ctrl Pts',(121.98624388122,4.90802428363638,335.34539473109));
#54741=CARTESIAN_POINT('Ctrl Pts',(121.978491907697,4.91383517012843,335.208343426364));
#54742=CARTESIAN_POINT('Ctrl Pts',(121.970743217139,4.91964359570659,335.071350162947));
#54743=CARTESIAN_POINT('Ctrl Pts',(121.962994526582,4.91972180043954,334.934043251389));
#54744=CARTESIAN_POINT('Ctrl Pts',(121.955245836024,4.91405627467309,334.796938453059));
#54745=CARTESIAN_POINT('Ctrl Pts',(121.947498757646,4.90839192766659,334.659862180527));
#54746=CARTESIAN_POINT('Ctrl Pts',(121.939751679269,4.8969862432901,334.522988327875));
#54747=CARTESIAN_POINT('Ctrl Pts',(121.932004600891,4.87987782964372,334.386831646078));
#54748=CARTESIAN_POINT('Ctrl Pts',(121.924257457585,4.86276927261236,334.250673823156));
#54749=CARTESIAN_POINT('Ctrl Pts',(121.916510314279,4.83995793971277,334.115233570902));
#54750=CARTESIAN_POINT('Ctrl Pts',(121.908763170973,4.81153416580831,333.981019120023));
#54751=CARTESIAN_POINT('Ctrl Pts',(121.901014285945,4.78310400163598,333.846774494885));
#54752=CARTESIAN_POINT('Ctrl Pts',(121.893265400917,4.74905896659284,333.713756601827));
#54753=CARTESIAN_POINT('Ctrl Pts',(121.885516515889,4.70954013437084,333.582461716478));
#54754=CARTESIAN_POINT('Ctrl Pts',(121.877759406114,4.66997935645208,333.451027473381));
#54755=CARTESIAN_POINT('Ctrl Pts',(121.87000229634,4.62493328828028,333.321320266108));
#54756=CARTESIAN_POINT('Ctrl Pts',(121.862245186565,4.57459253821262,333.193820005695));
#54757=CARTESIAN_POINT('Ctrl Pts',(121.854483931639,4.52422488765774,333.066251613219));
#54758=CARTESIAN_POINT('Ctrl Pts',(121.846722676712,4.46855707611087,332.940892874562));
#54759=CARTESIAN_POINT('Ctrl Pts',(121.838961421786,4.40782676306542,332.818201134544));
#54760=CARTESIAN_POINT('Ctrl Pts',(121.831187751382,4.34699930131107,332.695313127728));
#54761=CARTESIAN_POINT('Ctrl Pts',(121.823414080977,4.28109334315855,332.575100987863));
#54762=CARTESIAN_POINT('Ctrl Pts',(121.815640410572,4.21039160983818,332.457995760369));
#54763=CARTESIAN_POINT('Ctrl Pts',(121.808228606395,4.14298105921344,332.346341809388));
#54764=CARTESIAN_POINT('Ctrl Pts',(121.800816802218,4.07121133062631,332.237512266963));
#54765=CARTESIAN_POINT('Ctrl Pts',(121.793404998041,3.9953616169164,332.131852756121));
#54766=CARTESIAN_POINT('Ctrl Pts',(121.785629919263,3.91579428279319,332.02101455791));
#54767=CARTESIAN_POINT('Ctrl Pts',(121.777854840484,3.83148545901994,331.913314724682));
#54768=CARTESIAN_POINT('Ctrl Pts',(121.770079761706,3.74271114088354,331.809185624577));
#54769=CARTESIAN_POINT('Ctrl Pts',(121.762314250657,3.65404606519725,331.705184661959));
#54770=CARTESIAN_POINT('Ctrl Pts',(121.754548739608,3.56092667993508,331.604745984242));
#54771=CARTESIAN_POINT('Ctrl Pts',(121.746783228559,3.46367192992948,331.508272658938));
#54772=CARTESIAN_POINT('Ctrl Pts',(121.739025417036,3.36651360829175,331.411894987217));
#54773=CARTESIAN_POINT('Ctrl Pts',(121.731267605514,3.2652283573074,331.319475117187));
#54774=CARTESIAN_POINT('Ctrl Pts',(121.723509793992,3.16017478153703,331.231382426852));
#54775=CARTESIAN_POINT('Ctrl Pts',(121.715757820469,3.05520026191402,331.143356029061));
#54776=CARTESIAN_POINT('Ctrl Pts',(121.708005846946,2.94646336029635,331.059650579522));
#54777=CARTESIAN_POINT('Ctrl Pts',(121.700253873423,2.83435859840053,330.980597756112));
#54778=CARTESIAN_POINT('Ctrl Pts',(121.692505182865,2.72230131293766,330.901578411619));
#54779=CARTESIAN_POINT('Ctrl Pts',(121.684756492308,2.60687932276282,330.827207999078));
#54780=CARTESIAN_POINT('Ctrl Pts',(121.67700780175,2.48851903176425,330.757776987115));
#54781=CARTESIAN_POINT('Ctrl Pts',(121.669260723372,2.37018336661294,330.688360420855));
#54782=CARTESIAN_POINT('Ctrl Pts',(121.661513644995,2.24891095356835,330.623881408687));
#54783=CARTESIAN_POINT('Ctrl Pts',(121.653766566617,2.12515555076475,330.564586045525));
#54784=CARTESIAN_POINT('Ctrl Pts',(121.646019423311,2.00139911077143,330.50529018541));
#54785=CARTESIAN_POINT('Ctrl Pts',(121.638272280005,1.87515999201355,330.451178229849));
#54786=CARTESIAN_POINT('Ctrl Pts',(121.630525136699,1.74691446191379,330.402449247126));
#54787=CARTESIAN_POINT('Ctrl Pts',(121.622776251671,1.61864009949674,330.353709309092));
#54788=CARTESIAN_POINT('Ctrl Pts',(121.615027366643,1.48835879344688,330.31035489088));
#54789=CARTESIAN_POINT('Ctrl Pts',(121.607278481615,1.35656421559843,330.272535923832));
#54790=CARTESIAN_POINT('Ctrl Pts',(121.59952137184,1.22462974962296,330.234676815341));
#54791=CARTESIAN_POINT('Ctrl Pts',(121.591764262066,1.0911791796142,330.202365002629));
#54792=CARTESIAN_POINT('Ctrl Pts',(121.584007152291,0.956719222120495,330.175699906461));
#54793=CARTESIAN_POINT('Ctrl Pts',(121.576245897365,0.822187413524834,330.149020561317));
#54794=CARTESIAN_POINT('Ctrl Pts',(121.568484642439,0.686645528730564,330.127994005098));
#54795=CARTESIAN_POINT('Ctrl Pts',(121.560723387512,0.550606769942869,330.112667880388));
#54796=CARTESIAN_POINT('Ctrl Pts',(121.552949717108,0.414350393475856,330.097317238873));
#54797=CARTESIAN_POINT('Ctrl Pts',(121.545176046703,0.277595944810239,330.087685278473));
#54798=CARTESIAN_POINT('Ctrl Pts',(121.537402376298,0.140858895915563,330.083767516284));
#54799=CARTESIAN_POINT('Ctrl Pts',(121.529990572121,0.0104869895433629,
330.080032126868));
#54800=CARTESIAN_POINT('Ctrl Pts',(121.522578767944,-0.119868812743053,
330.081490912733));
#54801=CARTESIAN_POINT('Ctrl Pts',(121.515166963767,-0.249766781901038,
330.088096131116));
#54802=CARTESIAN_POINT('Ctrl Pts',(121.507391884989,-0.386031437473093,
330.095025090928));
#54803=CARTESIAN_POINT('Ctrl Pts',(121.49961680621,-0.522222867092972,330.107639619914));
#54804=CARTESIAN_POINT('Ctrl Pts',(121.491841727432,-0.657828126280897,
330.125941606959));
#54805=CARTESIAN_POINT('Ctrl Pts',(121.484076216383,-0.793266514564706,
330.144221072244));
#54806=CARTESIAN_POINT('Ctrl Pts',(121.476310705334,-0.928119783977434,
330.168174018243));
#54807=CARTESIAN_POINT('Ctrl Pts',(121.468545194285,-1.06187638709854,330.197750360402));
#54808=CARTESIAN_POINT('Ctrl Pts',(121.460787382762,-1.19550037015804,330.227297377531));
#54809=CARTESIAN_POINT('Ctrl Pts',(121.45302957124,-1.32802947161284,330.262456611185));
#54810=CARTESIAN_POINT('Ctrl Pts',(121.445271759718,-1.45895901211281,330.303126394773));
#54811=CARTESIAN_POINT('Ctrl Pts',(121.437519786195,-1.58979002398029,330.343765573059));
#54812=CARTESIAN_POINT('Ctrl Pts',(121.429767812672,-1.71902349906192,330.389906931666));
#54813=CARTESIAN_POINT('Ctrl Pts',(121.422015839149,-1.84616702401678,330.441398198797));
#54814=CARTESIAN_POINT('Ctrl Pts',(121.414267148591,-1.97325670361412,330.492867659346));
#54815=CARTESIAN_POINT('Ctrl Pts',(121.406518458034,-2.098257831939,330.549682375705));
#54816=CARTESIAN_POINT('Ctrl Pts',(121.398769767476,-2.22069539611521,330.611640964988));
#54817=CARTESIAN_POINT('Ctrl Pts',(121.391022689098,-2.34310748613375,330.673586663269));
#54818=CARTESIAN_POINT('Ctrl Pts',(121.38327561072,-2.46295672437351,330.740673929343));
#54819=CARTESIAN_POINT('Ctrl Pts',(121.375528532343,-2.57979060980841,330.812654364392));
#54820=CARTESIAN_POINT('Ctrl Pts',(121.367781389037,-2.69662547442369,330.884635402707));
#54821=CARTESIAN_POINT('Ctrl Pts',(121.360034245731,-2.81044460304188,330.961509486766));
#54822=CARTESIAN_POINT('Ctrl Pts',(121.352287102425,-2.92082285926509,331.042983840405));
#54823=CARTESIAN_POINT('Ctrl Pts',(121.344538217397,-3.03122593086363,331.124476511209));
#54824=CARTESIAN_POINT('Ctrl Pts',(121.336789332369,-3.13818627630762,331.210571277526));
#54825=CARTESIAN_POINT('Ctrl Pts',(121.329040447341,-3.24131066097623,331.300934136631));
#54826=CARTESIAN_POINT('Ctrl Pts',(121.321283337566,-3.34454450293235,331.391392907809));
#54827=CARTESIAN_POINT('Ctrl Pts',(121.313526227791,-3.44393395640828,331.486128563262));
#54828=CARTESIAN_POINT('Ctrl Pts',(121.305769118017,-3.53912120296185,331.584768796517));
#54829=CARTESIAN_POINT('Ctrl Pts',(121.298007863091,-3.63435931453638,331.683461739958));
#54830=CARTESIAN_POINT('Ctrl Pts',(121.290246608164,-3.72539048549737,331.786063126467));
#54831=CARTESIAN_POINT('Ctrl Pts',(121.282485353238,-3.81189692901671,331.892167175498));
#54832=CARTESIAN_POINT('Ctrl Pts',(121.274711682834,-3.89854175465324,331.998440956428));
#54833=CARTESIAN_POINT('Ctrl Pts',(121.266938012429,-3.9806471547837,332.108228283385));
#54834=CARTESIAN_POINT('Ctrl Pts',(121.259164342024,-4.05793794771738,332.221093259036));
#54835=CARTESIAN_POINT('Ctrl Pts',(121.251752537847,-4.13163083564451,332.328704342916));
#54836=CARTESIAN_POINT('Ctrl Pts',(121.24434073367,-4.20094711591959,332.439112750813));
#54837=CARTESIAN_POINT('Ctrl Pts',(121.236928929493,-4.26568789151947,332.551921187003));
#54838=CARTESIAN_POINT('Ctrl Pts',(121.228828213401,-4.33644618871474,332.675214934724));
#54839=CARTESIAN_POINT('Ctrl Pts',(121.220727497309,-4.40194677956996,332.801737972689));
#54840=CARTESIAN_POINT('Ctrl Pts',(121.212626781217,-4.46189582822964,332.931022310288));
#54841=CARTESIAN_POINT('Ctrl Pts',(121.20453903916,-4.52174886302869,333.060099587247));
#54842=CARTESIAN_POINT('Ctrl Pts',(121.196451297102,-4.57606792476237,333.191929043033));
#54843=CARTESIAN_POINT('Ctrl Pts',(121.188363555044,-4.62460398813504,333.326016423191));
#54844=CARTESIAN_POINT('Ctrl Pts',(121.180292334472,-4.67304090296312,333.459829892206));
#54845=CARTESIAN_POINT('Ctrl Pts',(121.1722211139,-4.71571825763362,333.595891766523));
#54846=CARTESIAN_POINT('Ctrl Pts',(121.164149893328,-4.75243452649791,333.733686794726));
#54847=CARTESIAN_POINT('Ctrl Pts',(121.156088312233,-4.78910694503617,333.871317254004));
#54848=CARTESIAN_POINT('Ctrl Pts',(121.148026731138,-4.81983236969226,334.010676413363));
#54849=CARTESIAN_POINT('Ctrl Pts',(121.139965150044,-4.84445818720349,334.151231518648));
#54850=CARTESIAN_POINT('Ctrl Pts',(121.13191558772,-4.86904729081765,334.291577074517));
#54851=CARTESIAN_POINT('Ctrl Pts',(121.123866025396,-4.8875548596542,334.433114683237));
#54852=CARTESIAN_POINT('Ctrl Pts',(121.115816463072,-4.89987883100826,334.575299512671));
#54853=CARTESIAN_POINT('Ctrl Pts',(121.107816767551,-4.91212645572145,334.716603511261));
#54854=CARTESIAN_POINT('Ctrl Pts',(121.099817072029,-4.91826683467075,334.858546396624));
#54855=CARTESIAN_POINT('Ctrl Pts',(121.091817376508,-4.91824996531272,335.00058412452));
#54856=CARTESIAN_POINT('',(119.341817376544,-4.91824813200487,335.004286552297));
#54857=CARTESIAN_POINT('Ctrl Pts',(121.091817376452,-4.9182499653126,335.000584125506));
#54858=CARTESIAN_POINT('Ctrl Pts',(121.083626109023,-4.91823269194814,335.14602328768));
#54859=CARTESIAN_POINT('Ctrl Pts',(121.075434841593,-4.91175990151259,335.291314156804));
#54860=CARTESIAN_POINT('Ctrl Pts',(121.067243574164,-4.89889653869584,335.435885037199));
#54861=CARTESIAN_POINT('Ctrl Pts',(121.059038712186,-4.88601182733872,335.580695853086));
#54862=CARTESIAN_POINT('Ctrl Pts',(121.050833850209,-4.866715397838,335.724783977587));
#54863=CARTESIAN_POINT('Ctrl Pts',(121.042628988231,-4.84112349270298,335.867586532226));
#54864=CARTESIAN_POINT('Ctrl Pts',(121.034402112649,-4.81546292461099,336.010772225424));
#54865=CARTESIAN_POINT('Ctrl Pts',(121.026175237067,-4.78347315885324,336.152665136094));
#54866=CARTESIAN_POINT('Ctrl Pts',(121.017948361485,-4.74532117486993,336.292714202688));
#54867=CARTESIAN_POINT('Ctrl Pts',(121.009709509761,-4.70711365174982,336.432967143457));
#54868=CARTESIAN_POINT('Ctrl Pts',(121.001470658036,-4.66272609908869,336.571370578572));
#54869=CARTESIAN_POINT('Ctrl Pts',(120.993231806312,-4.61237422615327,336.707391888354));
#54870=CARTESIAN_POINT('Ctrl Pts',(120.98497374741,-4.56190496824396,336.843730303677));
#54871=CARTESIAN_POINT('Ctrl Pts',(120.976715688508,-4.50544371147639,336.977675195475));
#54872=CARTESIAN_POINT('Ctrl Pts',(120.968457629606,-4.44325357566152,337.108715420551));
#54873=CARTESIAN_POINT('Ctrl Pts',(120.965202051477,-4.41873633155052,337.160375465098));
#54874=CARTESIAN_POINT('Ctrl Pts',(120.961946473348,-4.39332920629337,337.211584371123));
#54875=CARTESIAN_POINT('Ctrl Pts',(120.958690895219,-4.36705018454127,337.262312035993));
#54876=CARTESIAN_POINT('Ctrl Pts',(120.950915816441,-4.30428976035348,337.383461513903));
#54877=CARTESIAN_POINT('Ctrl Pts',(120.943140737662,-4.23638500062128,337.502188829417));
#54878=CARTESIAN_POINT('Ctrl Pts',(120.935365658884,-4.16354669774589,337.618026347879));
#54879=CARTESIAN_POINT('Ctrl Pts',(120.927600147835,-4.09079802703937,337.7337213209));
#54880=CARTESIAN_POINT('Ctrl Pts',(120.919834636786,-4.01312809889304,337.846533244715));
#54881=CARTESIAN_POINT('Ctrl Pts',(120.912069125737,-3.93079443009848,337.956017288652));
#54882=CARTESIAN_POINT('Ctrl Pts',(120.904311314215,-3.84854239537604,338.06539277884));
#54883=CARTESIAN_POINT('Ctrl Pts',(120.896553502693,-3.7616360556645,338.17144664516));
#54884=CARTESIAN_POINT('Ctrl Pts',(120.88879569117,-3.67037702928781,338.273761678158));
#54885=CARTESIAN_POINT('Ctrl Pts',(120.881043717647,-3.57918667822284,338.375999715849));
#54886=CARTESIAN_POINT('Ctrl Pts',(120.873291744124,-3.48365041941673,338.474504230006));
#54887=CARTESIAN_POINT('Ctrl Pts',(120.865539770601,-3.38411084731969,338.568890140583));
#54888=CARTESIAN_POINT('Ctrl Pts',(120.857791080044,-3.28461343029036,338.663236078672));
#54889=CARTESIAN_POINT('Ctrl Pts',(120.850042389486,-3.18111635505688,338.753466613945));
#54890=CARTESIAN_POINT('Ctrl Pts',(120.842293698929,-3.07399970514535,338.839232849837));
#54891=CARTESIAN_POINT('Ctrl Pts',(120.834546620551,-2.96690534174746,338.924981241347));
#54892=CARTESIAN_POINT('Ctrl Pts',(120.826799542173,-2.85619320653498,339.006266936845));
#54893=CARTESIAN_POINT('Ctrl Pts',(120.819052463795,-2.74227684758727,339.082781007314));
#54894=CARTESIAN_POINT('Ctrl Pts',(120.811305320489,-2.62835953391086,339.159295719045));
#54895=CARTESIAN_POINT('Ctrl Pts',(120.803558177183,-2.51123826741195,339.231038508042));
#54896=CARTESIAN_POINT('Ctrl Pts',(120.795811033878,-2.39135564874566,339.297743736394));
#54897=CARTESIAN_POINT('Ctrl Pts',(120.788062148849,-2.27144607792167,339.364463961497));
#54898=CARTESIAN_POINT('Ctrl Pts',(120.780313263821,-2.14877426107984,339.426144182292));
#54899=CARTESIAN_POINT('Ctrl Pts',(120.772564378793,-2.02380710405849,339.482564876057));
#54900=CARTESIAN_POINT('Ctrl Pts',(120.764807269019,-1.89870730560532,339.53904545533));
#54901=CARTESIAN_POINT('Ctrl Pts',(120.757050159244,-1.77130765705046,339.590255194877));
#54902=CARTESIAN_POINT('Ctrl Pts',(120.749293049469,-1.64209525323747,339.636022674858));
#54903=CARTESIAN_POINT('Ctrl Pts',(120.741531794543,-1.51281380244726,339.681814611516));
#54904=CARTESIAN_POINT('Ctrl Pts',(120.733770539617,-1.38171803961448,339.722158378908));
#54905=CARTESIAN_POINT('Ctrl Pts',(120.726009284691,-1.24930894073323,339.756932859848));
#54906=CARTESIAN_POINT('Ctrl Pts',(120.718235614286,-1.11668803044583,339.791762968625));
#54907=CARTESIAN_POINT('Ctrl Pts',(120.710461943881,-0.982749967949554,
339.821005904622));
#54908=CARTESIAN_POINT('Ctrl Pts',(120.702688273476,-0.848005488581748,
339.844591804666));
#54909=CARTESIAN_POINT('Ctrl Pts',(120.695276469299,-0.719533397145381,
339.867079775389));
#54910=CARTESIAN_POINT('Ctrl Pts',(120.687864665122,-0.590328561915231,
339.884425489532));
#54911=CARTESIAN_POINT('Ctrl Pts',(120.680452860945,-0.460834980762146,
339.896612521224));
#54912=CARTESIAN_POINT('Ctrl Pts',(120.672677782167,-0.3249945334561,339.909396875642));
#54913=CARTESIAN_POINT('Ctrl Pts',(120.664902703388,-0.188407039038985,
339.916544477495));
#54914=CARTESIAN_POINT('Ctrl Pts',(120.65712762461,-0.0515798133325195,
339.917979522665));
#54915=CARTESIAN_POINT('Ctrl Pts',(120.649362113561,0.0850790377618662,
339.919412801921));
#54916=CARTESIAN_POINT('Ctrl Pts',(120.641596602512,0.22197664605461,339.915147507451));
#54917=CARTESIAN_POINT('Ctrl Pts',(120.633831091463,0.35859958683003,339.905159467217));
#54918=CARTESIAN_POINT('Ctrl Pts',(120.62607327994,0.495087065561858,339.895181330153));
#54919=CARTESIAN_POINT('Ctrl Pts',(120.618315468418,0.63130003141299,339.87949176746));
#54920=CARTESIAN_POINT('Ctrl Pts',(120.610557656896,0.766724421070416,339.858118640445));
#54921=CARTESIAN_POINT('Ctrl Pts',(120.602805683373,0.902046899580025,339.836761597385));
#54922=CARTESIAN_POINT('Ctrl Pts',(120.59505370985,1.03658159854575,339.809729563976));
#54923=CARTESIAN_POINT('Ctrl Pts',(120.587301736327,1.16981929842708,339.777102246292));
#54924=CARTESIAN_POINT('Ctrl Pts',(120.579553045769,1.3030005720634,339.744488746296));
#54925=CARTESIAN_POINT('Ctrl Pts',(120.571804355212,1.43488556022777,339.706284767782));
#54926=CARTESIAN_POINT('Ctrl Pts',(120.564055664654,1.56497518335109,339.662621123145));
#54927=CARTESIAN_POINT('Ctrl Pts',(120.556308586276,1.69503774024178,339.618966563093));
#54928=CARTESIAN_POINT('Ctrl Pts',(120.548561507898,1.82330530476455,339.569854720659));
#54929=CARTESIAN_POINT('Ctrl Pts',(120.540814429521,1.94929429732398,339.515466178029));
#54930=CARTESIAN_POINT('Ctrl Pts',(120.533067286215,2.07528434579248,339.461077179569));
#54931=CARTESIAN_POINT('Ctrl Pts',(120.525320142909,2.19899542534465,339.401411547624));
#54932=CARTESIAN_POINT('Ctrl Pts',(120.517572999603,2.31996463878292,339.336697722611));
#54933=CARTESIAN_POINT('Ctrl Pts',(120.509824114575,2.44096104866867,339.271969348555));
#54934=CARTESIAN_POINT('Ctrl Pts',(120.502075229547,2.55921402122576,339.202190707367));
#54935=CARTESIAN_POINT('Ctrl Pts',(120.494326344519,2.67428628557384,339.127635633785));
#54936=CARTESIAN_POINT('Ctrl Pts',(120.486569234744,2.78948068881218,339.053001426678));
#54937=CARTESIAN_POINT('Ctrl Pts',(120.478812124969,2.90148731133285,338.973580872739));
#54938=CARTESIAN_POINT('Ctrl Pts',(120.471055015195,3.00989840756412,338.889690815302));
#54939=CARTESIAN_POINT('Ctrl Pts',(120.463293760269,3.1183674352189,338.8057559297));
#54940=CARTESIAN_POINT('Ctrl Pts',(120.455532505342,3.22323680945756,338.717347033389));
#54941=CARTESIAN_POINT('Ctrl Pts',(120.447771250416,3.32413357339789,338.624819864312));
#54942=CARTESIAN_POINT('Ctrl Pts',(120.439997580012,3.42519173927832,338.532144681918));
#54943=CARTESIAN_POINT('Ctrl Pts',(120.432223909607,3.52226431900991,338.435338338349));
#54944=CARTESIAN_POINT('Ctrl Pts',(120.424450239202,3.61501617496263,338.334792514874));
#54945=CARTESIAN_POINT('Ctrl Pts',(120.417038435025,3.70345040970563,338.238927123672));
#54946=CARTESIAN_POINT('Ctrl Pts',(120.409626630848,3.78795694089722,338.139662782483));
#54947=CARTESIAN_POINT('Ctrl Pts',(120.402214826671,3.86828168294719,338.037363969608));
#54948=CARTESIAN_POINT('Ctrl Pts',(120.394439747893,3.95254337988039,337.930051187182));
#54949=CARTESIAN_POINT('Ctrl Pts',(120.386664669114,4.0324692813839,337.819059826652));
#54950=CARTESIAN_POINT('Ctrl Pts',(120.378889590336,4.10772110445711,337.704775478759));
#54951=CARTESIAN_POINT('Ctrl Pts',(120.371124079287,4.18288032537127,337.590631765032));
#54952=CARTESIAN_POINT('Ctrl Pts',(120.363358568238,4.25337669928546,337.473203450056));
#54953=CARTESIAN_POINT('Ctrl Pts',(120.355593057189,4.31891205584332,337.352909202751));
#54954=CARTESIAN_POINT('Ctrl Pts',(120.347835245667,4.38438243390441,337.232734227543));
#54955=CARTESIAN_POINT('Ctrl Pts',(120.340077434145,4.44490139763382,337.109699315942));
#54956=CARTESIAN_POINT('Ctrl Pts',(120.332319622622,4.50021418704429,336.984251832108));
#54957=CARTESIAN_POINT('Ctrl Pts',(120.324567649099,4.55548535182662,336.858898751485));
#54958=CARTESIAN_POINT('Ctrl Pts',(120.316815675576,4.60555798343984,336.731137068577));
#54959=CARTESIAN_POINT('Ctrl Pts',(120.309063702053,4.65022354050941,336.601438130491));
#54960=CARTESIAN_POINT('Ctrl Pts',(120.301315011496,4.69487018168905,336.471794119983));
#54961=CARTESIAN_POINT('Ctrl Pts',(120.293566320938,4.73411417576512,336.340214854875));
#54962=CARTESIAN_POINT('Ctrl Pts',(120.285817630381,4.76779544507966,336.207190811917));
#54963=CARTESIAN_POINT('Ctrl Pts',(120.278070552003,4.8014697067248,336.074194445723));
#54964=CARTESIAN_POINT('Ctrl Pts',(120.270323473625,4.82958344982151,335.93975427827));
#54965=CARTESIAN_POINT('Ctrl Pts',(120.262576395247,4.85202683711541,335.804374685338));
#54966=CARTESIAN_POINT('Ctrl Pts',(120.254829251941,4.8744704125065,335.668993957794));
#54967=CARTESIAN_POINT('Ctrl Pts',(120.247082108636,4.89124347337942,335.53267417468));
#54968=CARTESIAN_POINT('Ctrl Pts',(120.23933496533,4.90228761992001,335.395928218341));
#54969=CARTESIAN_POINT('Ctrl Pts',(120.231586080302,4.91333424941921,335.259151518609));
#54970=CARTESIAN_POINT('Ctrl Pts',(120.223837195274,4.91864937018671,335.121948844524));
#54971=CARTESIAN_POINT('Ctrl Pts',(120.216088310246,4.91822662333291,334.984836094191));
#54972=CARTESIAN_POINT('Ctrl Pts',(120.208331200471,4.91780342777122,334.847577810967));
#54973=CARTESIAN_POINT('Ctrl Pts',(120.200574090696,4.91163019998556,334.710410033646));
#54974=CARTESIAN_POINT('Ctrl Pts',(120.192816980921,4.89975272576887,334.573847106286));
#54975=CARTESIAN_POINT('Ctrl Pts',(120.185055725995,4.88786890460974,334.437211204065));
#54976=CARTESIAN_POINT('Ctrl Pts',(120.177294471069,4.87027481338499,334.301181183282));
#54977=CARTESIAN_POINT('Ctrl Pts',(120.169533216143,4.84706777135025,334.166263181551));
#54978=CARTESIAN_POINT('Ctrl Pts',(120.161759545738,4.82382360561142,334.031129354987));
#54979=CARTESIAN_POINT('Ctrl Pts',(120.153985875334,4.79494862894768,333.897111484485));
#54980=CARTESIAN_POINT('Ctrl Pts',(120.146212204929,4.76059085229275,333.76470335564));
#54981=CARTESIAN_POINT('Ctrl Pts',(120.138800400752,4.72783243840713,333.638458857048));
#54982=CARTESIAN_POINT('Ctrl Pts',(120.131388596575,4.69009026920121,333.513677881297));
#54983=CARTESIAN_POINT('Ctrl Pts',(120.123976792398,4.64753334196125,333.390771334503));
#54984=CARTESIAN_POINT('Ctrl Pts',(120.116201713619,4.60289057294669,333.26184077173));
#54985=CARTESIAN_POINT('Ctrl Pts',(120.108426634841,4.55280806143128,333.134565582146));
#54986=CARTESIAN_POINT('Ctrl Pts',(120.100651556063,4.49742699455212,333.009438900417));
#54987=CARTESIAN_POINT('Ctrl Pts',(120.092886045014,4.44211407760149,332.884466195036));
#54988=CARTESIAN_POINT('Ctrl Pts',(120.085120533965,4.38151573532091,332.761637090968));
#54989=CARTESIAN_POINT('Ctrl Pts',(120.077355022916,4.31582267824842,332.641428891804));
#54990=CARTESIAN_POINT('Ctrl Pts',(120.069597211393,4.25019475603324,332.521339879419));
#54991=CARTESIAN_POINT('Ctrl Pts',(120.061839399871,4.17948235788482,332.403866941295));
#54992=CARTESIAN_POINT('Ctrl Pts',(120.054081588349,4.10392381662172,332.289466404955));
#54993=CARTESIAN_POINT('Ctrl Pts',(120.046329614826,4.02842213555707,332.175151958648));
#54994=CARTESIAN_POINT('Ctrl Pts',(120.038577641303,3.94808178485716,332.063905636886));
#54995=CARTESIAN_POINT('Ctrl Pts',(120.03082566778,3.86318627665475,331.956157879527));
#54996=CARTESIAN_POINT('Ctrl Pts',(120.023076977222,3.77832672175049,331.848455753407));
#54997=CARTESIAN_POINT('Ctrl Pts',(120.015328286665,3.68891608761505,331.744249551188));
#54998=CARTESIAN_POINT('Ctrl Pts',(120.007579596107,3.59528019940558,331.6439393107));
#54999=CARTESIAN_POINT('Ctrl Pts',(119.999832517729,3.50166379292471,331.543649940597));
#55000=CARTESIAN_POINT('Ctrl Pts',(119.992085439351,3.40382414751369,331.447255205462));
#55001=CARTESIAN_POINT('Ctrl Pts',(119.984338360974,3.3021259642863,331.355120416463));
#55002=CARTESIAN_POINT('Ctrl Pts',(119.976591217668,3.20042692873025,331.262984855286));
#55003=CARTESIAN_POINT('Ctrl Pts',(119.968844074362,3.09486958053087,331.175109573889));
#55004=CARTESIAN_POINT('Ctrl Pts',(119.961096931056,2.98585360990486,331.091821231991));
#55005=CARTESIAN_POINT('Ctrl Pts',(119.953348046028,2.87681313017418,331.008514165105));
#55006=CARTESIAN_POINT('Ctrl Pts',(119.945599161,2.76431279127489,330.929796327023));
#55007=CARTESIAN_POINT('Ctrl Pts',(119.937850275972,2.64878298176728,330.855952247138));
#55008=CARTESIAN_POINT('Ctrl Pts',(119.930093166197,2.53313054772618,330.782029788383));
#55009=CARTESIAN_POINT('Ctrl Pts',(119.922336056422,2.41444254965641,330.712991632335));
#55010=CARTESIAN_POINT('Ctrl Pts',(119.914578946648,2.29317628776919,330.649077617825));
#55011=CARTESIAN_POINT('Ctrl Pts',(119.906817691722,2.17184522506901,330.585129449709));
#55012=CARTESIAN_POINT('Ctrl Pts',(119.899056436795,2.04793350620948,330.526311046727));
#55013=CARTESIAN_POINT('Ctrl Pts',(119.891295181869,1.92191941813962,330.472814471145));
#55014=CARTESIAN_POINT('Ctrl Pts',(119.883521511465,1.79570374859674,330.419232318476));
#55015=CARTESIAN_POINT('Ctrl Pts',(119.87574784106,1.66737935542803,330.370989142701));
#55016=CARTESIAN_POINT('Ctrl Pts',(119.867974170655,1.53744157068174,330.328227693986));
#55017=CARTESIAN_POINT('Ctrl Pts',(119.860562366478,1.4135524210764,330.287456800996));
#55018=CARTESIAN_POINT('Ctrl Pts',(119.853150562301,1.28819698307923,330.251668850366));
#55019=CARTESIAN_POINT('Ctrl Pts',(119.845738758124,1.16181225053775,330.220944093547));
#55020=CARTESIAN_POINT('Ctrl Pts',(119.837963679345,1.02923302577381,330.188713424873));
#55021=CARTESIAN_POINT('Ctrl Pts',(119.830188600567,0.895102082840413,330.161952969137));
#55022=CARTESIAN_POINT('Ctrl Pts',(119.822413521789,0.759910513660583,330.140810862528));
#55023=CARTESIAN_POINT('Ctrl Pts',(119.81464801074,0.624885306313346,330.119694772627));
#55024=CARTESIAN_POINT('Ctrl Pts',(119.806882499691,0.488802452118738,330.104183335316));
#55025=CARTESIAN_POINT('Ctrl Pts',(119.799116988641,0.35216653026329,330.094374474396));
#55026=CARTESIAN_POINT('Ctrl Pts',(119.791359177119,0.215666083322119,330.084575338989));
#55027=CARTESIAN_POINT('Ctrl Pts',(119.783601365597,0.0786140473633463,
330.08046755576));
#55028=CARTESIAN_POINT('Ctrl Pts',(119.775843554075,-0.0584768664984696,
330.082097650564));
#55029=CARTESIAN_POINT('Ctrl Pts',(119.768091580552,-0.195464615099969,
330.083726518671));
#55030=CARTESIAN_POINT('Ctrl Pts',(119.760339607029,-0.33249079409725,330.091084665543));
#55031=CARTESIAN_POINT('Ctrl Pts',(119.752587633506,-0.469040012749843,
330.104166615484));
#55032=CARTESIAN_POINT('Ctrl Pts',(119.744838942948,-0.605531402727407,
330.117243025212));
#55033=CARTESIAN_POINT('Ctrl Pts',(119.737090252391,-0.741545845827129,
330.136038379577));
#55034=CARTESIAN_POINT('Ctrl Pts',(119.729341561833,-0.876570619014289,
330.160495168679));
#55035=CARTESIAN_POINT('Ctrl Pts',(119.721594483455,-1.01156729916968,330.184946869341));
#55036=CARTESIAN_POINT('Ctrl Pts',(119.713847405077,-1.14557433460566,330.215057592174));
#55037=CARTESIAN_POINT('Ctrl Pts',(119.706100326699,-1.2780871666694,330.250718343065));
#55038=CARTESIAN_POINT('Ctrl Pts',(119.698353183394,-1.41060110931822,330.286379392828));
#55039=CARTESIAN_POINT('Ctrl Pts',(119.690606040088,-1.54162044617135,330.32759046185));
#55040=CARTESIAN_POINT('Ctrl Pts',(119.682858896782,-1.67065418679368,330.374192216418));
#55041=CARTESIAN_POINT('Ctrl Pts',(119.675110011754,-1.79971693694032,330.42080444805));
#55042=CARTESIAN_POINT('Ctrl Pts',(119.667361126726,-1.92679283500087,330.472809644105));
#55043=CARTESIAN_POINT('Ctrl Pts',(119.659612241698,-2.05140970619441,330.529999856842));
#55044=CARTESIAN_POINT('Ctrl Pts',(119.651855131923,-2.17615884702256,330.587250771862));
#55045=CARTESIAN_POINT('Ctrl Pts',(119.644098022148,-2.29844339137983,330.64969753389));
#55046=CARTESIAN_POINT('Ctrl Pts',(119.636340912373,-2.4178141822908,330.717085379976));
#55047=CARTESIAN_POINT('Ctrl Pts',(119.628579657447,-2.53724876113577,330.784509235973));
#55048=CARTESIAN_POINT('Ctrl Pts',(119.620818402521,-2.6537661521668,330.85687923105));
#55049=CARTESIAN_POINT('Ctrl Pts',(119.613057147595,-2.76694601761512,330.93389709942));
#55050=CARTESIAN_POINT('Ctrl Pts',(119.60528347719,-2.88030693396285,331.01103817128));
#55051=CARTESIAN_POINT('Ctrl Pts',(119.597509806786,-2.9903193420906,331.092841740572));
#55052=CARTESIAN_POINT('Ctrl Pts',(119.589736136381,-3.09659514774521,331.178968522315));
#55053=CARTESIAN_POINT('Ctrl Pts',(119.582324332204,-3.1979237890775,331.261086081647));
#55054=CARTESIAN_POINT('Ctrl Pts',(119.574912528027,-3.29585566065839,331.3471332302));
#55055=CARTESIAN_POINT('Ctrl Pts',(119.56750072385,-3.39008679488294,331.436785919193));
#55056=CARTESIAN_POINT('Ctrl Pts',(119.559839911898,-3.48748372848824,331.529450589625));
#55057=CARTESIAN_POINT('Ctrl Pts',(119.552179099946,-3.58125425540994,331.62627909888));
#55058=CARTESIAN_POINT('Ctrl Pts',(119.544518287994,-3.6710133393594,331.726951860307));
#55059=CARTESIAN_POINT('Ctrl Pts',(119.536867029122,-3.76066049316255,331.827499082163));
#55060=CARTESIAN_POINT('Ctrl Pts',(119.529215770251,-3.84630588625596,331.931880724812));
#55061=CARTESIAN_POINT('Ctrl Pts',(119.52156451138,-3.9275989146357,332.039738216263));
#55062=CARTESIAN_POINT('Ctrl Pts',(119.513921918135,-4.00879987255432,332.147473551003));
#55063=CARTESIAN_POINT('Ctrl Pts',(119.506279324889,-4.0856580361039,332.258676578967));
#55064=CARTESIAN_POINT('Ctrl Pts',(119.498636731643,-4.1578614217354,332.372953852681));
#55065=CARTESIAN_POINT('Ctrl Pts',(119.490998992335,-4.23001894980219,332.487158547008));
#55066=CARTESIAN_POINT('Ctrl Pts',(119.483361253027,-4.29752736264881,332.604433265854));
#55067=CARTESIAN_POINT('Ctrl Pts',(119.475723513719,-4.36011666172829,332.724353771207));
#55068=CARTESIAN_POINT('Ctrl Pts',(119.468088858547,-4.42268068710995,332.844225852394));
#55069=CARTESIAN_POINT('Ctrl Pts',(119.460454203374,-4.48032936256405,332.966741238522));
#55070=CARTESIAN_POINT('Ctrl Pts',(119.452819548202,-4.53283781220414,333.091449652026));
#55071=CARTESIAN_POINT('Ctrl Pts',(119.44518621024,-4.58533720254364,333.216136549545));
#55072=CARTESIAN_POINT('Ctrl Pts',(119.437552872277,-4.63269797568408,333.343015349837));
#55073=CARTESIAN_POINT('Ctrl Pts',(119.429919534315,-4.67474296352263,333.471614810496));
#55074=CARTESIAN_POINT('Ctrl Pts',(119.42228264376,-4.7168075193005,333.600274121962));
#55075=CARTESIAN_POINT('Ctrl Pts',(119.414645753205,-4.75355121777498,333.730655311085));
#55076=CARTESIAN_POINT('Ctrl Pts',(119.407008862651,-4.78484645242896,333.862270906948));
#55077=CARTESIAN_POINT('Ctrl Pts',(119.399370303069,-4.81614852659181,333.993915267126));
#55078=CARTESIAN_POINT('Ctrl Pts',(119.391731743488,-4.84199968370608,334.126794176089));
#55079=CARTESIAN_POINT('Ctrl Pts',(119.384093183906,-4.8623235094944,334.26041014642));
#55080=CARTESIAN_POINT('Ctrl Pts',(119.376446474425,-4.88266901962485,334.394168677235));
#55081=CARTESIAN_POINT('Ctrl Pts',(119.368799764944,-4.89747536912074,334.52866543954));
#55082=CARTESIAN_POINT('Ctrl Pts',(119.361153055464,-4.90671803989672,334.663397653823));
#55083=CARTESIAN_POINT('Ctrl Pts',(119.354707829157,-4.91450846334283,334.77696017558));
#55084=CARTESIAN_POINT('Ctrl Pts',(119.348262602851,-4.91834713849611,334.890689783422));
#55085=CARTESIAN_POINT('Ctrl Pts',(119.341817376544,-4.91824813200487,335.004286552297));
#55086=CARTESIAN_POINT('',(117.59181737647,-4.91824919068085,334.99717849913));
#55087=CARTESIAN_POINT('Ctrl Pts',(119.341817376508,-4.91824813200431,335.00428655294));
#55088=CARTESIAN_POINT('Ctrl Pts',(119.330327476319,-4.91807163317883,335.206795429156));
#55089=CARTESIAN_POINT('Ctrl Pts',(119.318837576129,-4.90538450625377,335.408779786107));
#55090=CARTESIAN_POINT('Ctrl Pts',(119.30734767594,-4.88039897662853,335.609006478966));
#55091=CARTESIAN_POINT('Ctrl Pts',(119.301319347152,-4.86728998655602,335.714058073562));
#55092=CARTESIAN_POINT('Ctrl Pts',(119.295291018364,-4.85079630954624,335.818626478205));
#55093=CARTESIAN_POINT('Ctrl Pts',(119.289262689576,-4.83095322623972,335.922536713841));
#55094=CARTESIAN_POINT('Ctrl Pts',(119.281487610798,-4.80536047220388,336.056555659453));
#55095=CARTESIAN_POINT('Ctrl Pts',(119.273712532019,-4.7741461771936,336.18972059339));
#55096=CARTESIAN_POINT('Ctrl Pts',(119.265937453241,-4.73737897440254,336.321523180042));
#55097=CARTESIAN_POINT('Ctrl Pts',(119.258171942192,-4.70065701599525,336.45316357522));
#55098=CARTESIAN_POINT('Ctrl Pts',(119.250406431143,-4.65839584995196,336.583444585877));
#55099=CARTESIAN_POINT('Ctrl Pts',(119.242640920094,-4.61071539758645,336.711866403946));
#55100=CARTESIAN_POINT('Ctrl Pts',(119.234883108572,-4.56308222052834,336.840160891408));
#55101=CARTESIAN_POINT('Ctrl Pts',(119.227125297049,-4.51004058536871,336.966599490669));
#55102=CARTESIAN_POINT('Ctrl Pts',(119.219367485527,-4.4517605618634,337.090696286489));
#55103=CARTESIAN_POINT('Ctrl Pts',(119.211615512004,-4.39352439592375,337.214699695535));
#55104=CARTESIAN_POINT('Ctrl Pts',(119.203863538481,-4.33005785359038,337.336364456498));
#55105=CARTESIAN_POINT('Ctrl Pts',(119.196111564958,-4.26157944355582,337.455223759408));
#55106=CARTESIAN_POINT('Ctrl Pts',(119.1883628744,-4.19313003416872,337.574032725332));
#55107=CARTESIAN_POINT('Ctrl Pts',(119.180614183843,-4.11967317336198,337.690038258295));
#55108=CARTESIAN_POINT('Ctrl Pts',(119.172865493285,-4.04147362309771,337.802797533948));
#55109=CARTESIAN_POINT('Ctrl Pts',(119.165118414907,-3.96329034290301,337.915533349092));
#55110=CARTESIAN_POINT('Ctrl Pts',(119.15737133653,-3.88036655858897,338.025023929376));
#55111=CARTESIAN_POINT('Ctrl Pts',(119.149624258152,-3.79301050755723,338.13085521097));
#55112=CARTESIAN_POINT('Ctrl Pts',(119.141877114846,-3.70565372439767,338.236687379532));
#55113=CARTESIAN_POINT('Ctrl Pts',(119.13412997154,-3.61386484925101,338.338859886787));
#55114=CARTESIAN_POINT('Ctrl Pts',(119.126382828234,-3.517992314405,338.436991873468));
#55115=CARTESIAN_POINT('Ctrl Pts',(119.118633943206,-3.42209822537779,338.535145922304));
#55116=CARTESIAN_POINT('Ctrl Pts',(119.110885058178,-3.32211892284697,338.629257363426));
#55117=CARTESIAN_POINT('Ctrl Pts',(119.10313617315,-3.21843928947237,338.718982603143));
#55118=CARTESIAN_POINT('Ctrl Pts',(119.095379063375,-3.11464960946366,338.808803078157));
#55119=CARTESIAN_POINT('Ctrl Pts',(119.0876219536,-3.00715204895311,338.894227795661));
#55120=CARTESIAN_POINT('Ctrl Pts',(119.079864843826,-2.89636456285004,338.974953506843));
#55121=CARTESIAN_POINT('Ctrl Pts',(119.0721035889,-2.7855178754567,339.055722355265));
#55122=CARTESIAN_POINT('Ctrl Pts',(119.064342333973,-2.67137808453528,339.131786977321));
#55123=CARTESIAN_POINT('Ctrl Pts',(119.056581079047,-2.55439079901421,339.202888376868));
#55124=CARTESIAN_POINT('Ctrl Pts',(119.048807408643,-2.43721637196238,339.274103515483));
#55125=CARTESIAN_POINT('Ctrl Pts',(119.041033738238,-2.31718569035163,339.340339377091));
#55126=CARTESIAN_POINT('Ctrl Pts',(119.033260067833,-2.19476833798042,339.401383305859));
#55127=CARTESIAN_POINT('Ctrl Pts',(119.025848263656,-2.07804954281425,339.459585625057));
#55128=CARTESIAN_POINT('Ctrl Pts',(119.018436459479,-1.95916153794591,339.513068384374));
#55129=CARTESIAN_POINT('Ctrl Pts',(119.011024655302,-1.83852518662641,339.561689182818));
#55130=CARTESIAN_POINT('Ctrl Pts',(119.003249576524,-1.71197608837132,339.612693031428));
#55131=CARTESIAN_POINT('Ctrl Pts',(118.995474497745,-1.58310300836854,339.658507451582));
#55132=CARTESIAN_POINT('Ctrl Pts',(118.987699418967,-1.45237055823626,339.698915068829));
#55133=CARTESIAN_POINT('Ctrl Pts',(118.979933907918,-1.32179898270666,339.739272961931));
#55134=CARTESIAN_POINT('Ctrl Pts',(118.972168396869,-1.18937295953024,339.774237176192));
#55135=CARTESIAN_POINT('Ctrl Pts',(118.96440288582,-1.05557768427809,339.803638081179));
#55136=CARTESIAN_POINT('Ctrl Pts',(118.956645074297,-0.921915067430979,
339.833009835083));
#55137=CARTESIAN_POINT('Ctrl Pts',(118.948887262775,-0.786886279549922,
339.856829173589));
#55138=CARTESIAN_POINT('Ctrl Pts',(118.941129451253,-0.650991971630229,
339.874976155365));
#55139=CARTESIAN_POINT('Ctrl Pts',(118.93337747773,-0.515199928486656,339.893109480961));
#55140=CARTESIAN_POINT('Ctrl Pts',(118.925625504207,-0.378544047622639,
339.905578894793));
#55141=CARTESIAN_POINT('Ctrl Pts',(118.917873530684,-0.241535127094092,
339.912315527822));
#55142=CARTESIAN_POINT('Ctrl Pts',(118.910124840126,-0.104584229924731,
339.919049307883));
#55143=CARTESIAN_POINT('Ctrl Pts',(118.902376149569,0.0327190199491614,
339.920055116779));
#55144=CARTESIAN_POINT('Ctrl Pts',(118.894627459011,0.169858964197006,339.915315960829));
#55145=CARTESIAN_POINT('Ctrl Pts',(118.886880380633,0.306970375333988,339.910577790901));
#55146=CARTESIAN_POINT('Ctrl Pts',(118.879133302255,0.443918158031927,339.900097047129));
#55147=CARTESIAN_POINT('Ctrl Pts',(118.871386223877,0.580187312238033,339.883908859225));
#55148=CARTESIAN_POINT('Ctrl Pts',(118.863639080572,0.716457608510856,339.867720535648));
#55149=CARTESIAN_POINT('Ctrl Pts',(118.855891937266,0.852048876802527,339.84582471864));
#55150=CARTESIAN_POINT('Ctrl Pts',(118.84814479396,0.986452287726923,339.818308307543));
#55151=CARTESIAN_POINT('Ctrl Pts',(118.840395908932,1.12088591539142,339.790785710172));
#55152=CARTESIAN_POINT('Ctrl Pts',(118.832647023904,1.25413077142126,339.757640082614));
#55153=CARTESIAN_POINT('Ctrl Pts',(118.824898138876,1.38568963845844,339.719009142645));
#55154=CARTESIAN_POINT('Ctrl Pts',(118.817141029101,1.51738814343649,339.680337199398));
#55155=CARTESIAN_POINT('Ctrl Pts',(118.809383919326,1.6473967090434,339.636168423715));
#55156=CARTESIAN_POINT('Ctrl Pts',(118.801626809552,1.775234147499,339.586690177465));
#55157=CARTESIAN_POINT('Ctrl Pts',(118.793865554625,1.90313989819427,339.537185491622));
#55158=CARTESIAN_POINT('Ctrl Pts',(118.786104299699,2.0288718518561,339.482365837952));
#55159=CARTESIAN_POINT('Ctrl Pts',(118.778343044773,2.15197106854176,339.422465780835));
#55160=CARTESIAN_POINT('Ctrl Pts',(118.770569374368,2.27526720385618,339.362469903149));
#55161=CARTESIAN_POINT('Ctrl Pts',(118.762795703964,2.39592184214174,339.297377567569));
#55162=CARTESIAN_POINT('Ctrl Pts',(118.755022033559,2.51350203783212,339.227468576857));
#55163=CARTESIAN_POINT('Ctrl Pts',(118.747610229382,2.62560884712367,339.160813866482));
#55164=CARTESIAN_POINT('Ctrl Pts',(118.740198425205,2.73492076166339,339.089780996731));
#55165=CARTESIAN_POINT('Ctrl Pts',(118.732786621028,2.8410902801649,339.014646819143));
#55166=CARTESIAN_POINT('Ctrl Pts',(118.72501154225,2.95246348303192,338.935830091697));
#55167=CARTESIAN_POINT('Ctrl Pts',(118.717236463471,3.06073042467197,338.852250780912));
#55168=CARTESIAN_POINT('Ctrl Pts',(118.709461384693,3.16545688226668,338.764181954822));
#55169=CARTESIAN_POINT('Ctrl Pts',(118.701695873644,3.2700544672881,338.67622150303));
#55170=CARTESIAN_POINT('Ctrl Pts',(118.693930362595,3.3711199407333,338.583782777539));
#55171=CARTESIAN_POINT('Ctrl Pts',(118.686164851546,3.46824808958798,338.487181992895));
#55172=CARTESIAN_POINT('Ctrl Pts',(118.678407040023,3.5652799356003,338.39067698821));
#55173=CARTESIAN_POINT('Ctrl Pts',(118.670649228501,3.65838195058581,338.290018410587));
#55174=CARTESIAN_POINT('Ctrl Pts',(118.662891416979,3.74718234233851,338.185562360992));
#55175=CARTESIAN_POINT('Ctrl Pts',(118.655139443456,3.83591590898038,338.081184917886));
#55176=CARTESIAN_POINT('Ctrl Pts',(118.647387469933,3.92035404354363,337.973015987562));
#55177=CARTESIAN_POINT('Ctrl Pts',(118.63963549641,4.00016241044551,337.861447842013));
#55178=CARTESIAN_POINT('Ctrl Pts',(118.631886805852,4.07993697845662,337.749926945639));
#55179=CARTESIAN_POINT('Ctrl Pts',(118.624138115295,4.15508545158094,337.635010014491));
#55180=CARTESIAN_POINT('Ctrl Pts',(118.616389424737,4.2253144871583,337.517121480404));
#55181=CARTESIAN_POINT('Ctrl Pts',(118.608642346359,4.29552891099824,337.399257474011));
#55182=CARTESIAN_POINT('Ctrl Pts',(118.600895267982,4.36082573324415,337.278423430048));
#55183=CARTESIAN_POINT('Ctrl Pts',(118.593148189604,4.42095579913912,337.155071433748));
#55184=CARTESIAN_POINT('Ctrl Pts',(118.585401046298,4.48108636898191,337.03171840364));
#55185=CARTESIAN_POINT('Ctrl Pts',(118.577653902992,4.53604992483119,336.905847730457));
#55186=CARTESIAN_POINT('Ctrl Pts',(118.569906759686,4.58564418541981,336.777934325903));
#55187=CARTESIAN_POINT('Ctrl Pts',(118.562157874658,4.63524959585112,336.649992163701));
#55188=CARTESIAN_POINT('Ctrl Pts',(118.55440898963,4.6794831676924,336.520006720644));
#55189=CARTESIAN_POINT('Ctrl Pts',(118.546660104602,4.71819163791801,336.388470644407));
#55190=CARTESIAN_POINT('Ctrl Pts',(118.538902994827,4.75694119371387,336.25679495442));
#55191=CARTESIAN_POINT('Ctrl Pts',(118.531145885053,4.79015382268305,336.123565719065));
#55192=CARTESIAN_POINT('Ctrl Pts',(118.523388775278,4.81772668309809,335.989288971668));
#55193=CARTESIAN_POINT('Ctrl Pts',(118.515627520352,4.84531427756812,335.854940471071));
#55194=CARTESIAN_POINT('Ctrl Pts',(118.507866265426,4.86725603589562,335.719543728712));
#55195=CARTESIAN_POINT('Ctrl Pts',(118.500105010499,4.88350084953506,335.583611613224));
#55196=CARTESIAN_POINT('Ctrl Pts',(118.492331340095,4.89977164958214,335.447462050652));
#55197=CARTESIAN_POINT('Ctrl Pts',(118.48455766969,4.91032726384758,335.310775793485));
#55198=CARTESIAN_POINT('Ctrl Pts',(118.476783999286,4.9151686927531,335.174068332214));
#55199=CARTESIAN_POINT('Ctrl Pts',(118.469372195108,4.91978475197834,335.043724636154));
#55200=CARTESIAN_POINT('Ctrl Pts',(118.461960390931,4.91920664565874,334.91336195346));
#55201=CARTESIAN_POINT('Ctrl Pts',(118.454548586754,4.91347913127396,334.78342232563));
#55202=CARTESIAN_POINT('Ctrl Pts',(118.446773507976,4.90747089434785,334.647113969572));
#55203=CARTESIAN_POINT('Ctrl Pts',(118.438998429197,4.89577672329974,334.510840427728));
#55204=CARTESIAN_POINT('Ctrl Pts',(118.431223350419,4.87839126398238,334.37511462011));
#55205=CARTESIAN_POINT('Ctrl Pts',(118.42345783937,4.86102719857951,334.239555831739));
#55206=CARTESIAN_POINT('Ctrl Pts',(118.415692328321,4.83798582903697,334.104543820485));
#55207=CARTESIAN_POINT('Ctrl Pts',(118.407926817272,4.80931378289956,333.970590460452));
#55208=CARTESIAN_POINT('Ctrl Pts',(118.400169005749,4.78067016517937,333.836769915565));
#55209=CARTESIAN_POINT('Ctrl Pts',(118.392411194227,4.74640706230068,333.70400631278));
#55210=CARTESIAN_POINT('Ctrl Pts',(118.384653382705,4.70662272906663,333.572805006759));
#55211=CARTESIAN_POINT('Ctrl Pts',(118.376901409182,4.666868334805,333.441702433881));
#55212=CARTESIAN_POINT('Ctrl Pts',(118.369149435659,4.62160109328377,333.312160190188));
#55213=CARTESIAN_POINT('Ctrl Pts',(118.361397462136,4.57096994622283,333.184671706487));
#55214=CARTESIAN_POINT('Ctrl Pts',(118.353648771578,4.5203602414827,333.057237214235));
#55215=CARTESIAN_POINT('Ctrl Pts',(118.345900081021,4.46439129326101,332.931855114586));
#55216=CARTESIAN_POINT('Ctrl Pts',(118.338151390463,4.40326127079749,332.809001770061));
#55217=CARTESIAN_POINT('Ctrl Pts',(118.330404312085,4.34214396694569,332.6861739862));
#55218=CARTESIAN_POINT('Ctrl Pts',(118.322657233707,4.275867898744,332.565874260683));
#55219=CARTESIAN_POINT('Ctrl Pts',(118.31491015533,4.20467840237431,332.448556762319));
#55220=CARTESIAN_POINT('Ctrl Pts',(118.307163012024,4.13348830936811,332.331238280722));
#55221=CARTESIAN_POINT('Ctrl Pts',(118.299415868718,4.05738490883286,332.216902410295));
#55222=CARTESIAN_POINT('Ctrl Pts',(118.291668725412,3.97665809815358,332.105976255645));
#55223=CARTESIAN_POINT('Ctrl Pts',(118.283919840384,3.89591313837344,331.995025162441));
#55224=CARTESIAN_POINT('Ctrl Pts',(118.276170955356,3.81054293003373,331.887485626396));
#55225=CARTESIAN_POINT('Ctrl Pts',(118.268422070328,3.72087881165768,331.783753129585));
#55226=CARTESIAN_POINT('Ctrl Pts',(118.260664960553,3.63111952285988,331.679910530029));
#55227=CARTESIAN_POINT('Ctrl Pts',(118.252907850778,3.53705747580378,331.579883337826));
#55228=CARTESIAN_POINT('Ctrl Pts',(118.245150741004,3.43906255114998,331.484031878447));
#55229=CARTESIAN_POINT('Ctrl Pts',(118.237389486077,3.34101526114174,331.388129199113));
#55230=CARTESIAN_POINT('Ctrl Pts',(118.229628231151,3.23903119637746,331.296406960074));
#55231=CARTESIAN_POINT('Ctrl Pts',(118.221866976225,3.13351398126666,331.209185682244));
#55232=CARTESIAN_POINT('Ctrl Pts',(118.21409330582,3.02782797299966,331.121824878794));
#55233=CARTESIAN_POINT('Ctrl Pts',(118.206319635416,2.91859783183401,331.038979660755));
#55234=CARTESIAN_POINT('Ctrl Pts',(118.198545965011,2.80625758610726,330.960928148335));
#55235=CARTESIAN_POINT('Ctrl Pts',(118.191134160834,2.69914680584742,330.886509952596));
#55236=CARTESIAN_POINT('Ctrl Pts',(118.183722356657,2.5892091983047,330.81644936672));
#55237=CARTESIAN_POINT('Ctrl Pts',(118.17631055248,2.47684070644631,330.750947967206));
#55238=CARTESIAN_POINT('Ctrl Pts',(118.168535473702,2.35896470007272,330.682236148983));
#55239=CARTESIAN_POINT('Ctrl Pts',(118.160760394923,2.23804098450162,330.618324594035));
#55240=CARTESIAN_POINT('Ctrl Pts',(118.152985316145,2.1144979876788,330.55949537523));
#55241=CARTESIAN_POINT('Ctrl Pts',(118.145219805096,1.99110701837866,330.500738549524));
#55242=CARTESIAN_POINT('Ctrl Pts',(118.137454294047,1.86510353058753,330.447051782462));
#55243=CARTESIAN_POINT('Ctrl Pts',(118.129688782998,1.73694320299964,330.398672868394));
#55244=CARTESIAN_POINT('Ctrl Pts',(118.121930971475,1.60890994674965,330.35034192216));
#55245=CARTESIAN_POINT('Ctrl Pts',(118.114173159953,1.47872446979597,330.307308492901));
#55246=CARTESIAN_POINT('Ctrl Pts',(118.106415348431,1.34686490696827,330.269763432462));
#55247=CARTESIAN_POINT('Ctrl Pts',(118.098663374908,1.21510457264324,330.232246625871));
#55248=CARTESIAN_POINT('Ctrl Pts',(118.090911401385,1.08167303443826,330.200210073806));
#55249=CARTESIAN_POINT('Ctrl Pts',(118.083159427862,0.947065829757921,330.173795551719));
#55250=CARTESIAN_POINT('Ctrl Pts',(118.075410737304,0.812515631308635,330.147392216199));
#55251=CARTESIAN_POINT('Ctrl Pts',(118.067662046747,0.676791139423746,330.12660625026));
#55252=CARTESIAN_POINT('Ctrl Pts',(118.059913356189,0.540400178256569,330.111528796255));
#55253=CARTESIAN_POINT('Ctrl Pts',(118.052166277811,0.404037594368023,330.096454479241));
#55254=CARTESIAN_POINT('Ctrl Pts',(118.044419199434,0.26700920527441,330.087086354655));
#55255=CARTESIAN_POINT('Ctrl Pts',(118.036672121056,0.129829696703436,330.083463890873));
#55256=CARTESIAN_POINT('Ctrl Pts',(118.02892497775,-0.00735096156394813,
330.07984139673));
#55257=CARTESIAN_POINT('Ctrl Pts',(118.021177834444,-0.144682351096794,
330.081964669756));
#55258=CARTESIAN_POINT('Ctrl Pts',(118.013430691138,-0.281648430409271,
330.089821059865));
#55259=CARTESIAN_POINT('Ctrl Pts',(118.00568180611,-0.418645302604203,330.097679216257));
#55260=CARTESIAN_POINT('Ctrl Pts',(117.997932921082,-0.555276310993658,
330.111273032172));
#55261=CARTESIAN_POINT('Ctrl Pts',(117.990184036054,-0.691029579977796,
330.13053789602));
#55262=CARTESIAN_POINT('Ctrl Pts',(117.982426926279,-0.826926938884273,
330.149823207794));
#55263=CARTESIAN_POINT('Ctrl Pts',(117.974669816505,-0.961944309735628,
330.174791536629));
#55264=CARTESIAN_POINT('Ctrl Pts',(117.96691270673,-1.095578523506,330.205326834775));
#55265=CARTESIAN_POINT('Ctrl Pts',(117.959151451804,-1.22928414712742,330.235878450008));
#55266=CARTESIAN_POINT('Ctrl Pts',(117.951390196878,-1.36160476403147,330.272002859238));
#55267=CARTESIAN_POINT('Ctrl Pts',(117.943628941951,-1.49205241701669,330.313534098345));
#55268=CARTESIAN_POINT('Ctrl Pts',(117.935855271547,-1.62270874373381,330.3551317739));
#55269=CARTESIAN_POINT('Ctrl Pts',(117.928081601142,-1.75148575201679,330.40215342879));
#55270=CARTESIAN_POINT('Ctrl Pts',(117.920307930737,-1.87791468701139,330.454384586131));
#55271=CARTESIAN_POINT('Ctrl Pts',(117.91289612656,-1.9984583246656,330.504184370531));
#55272=CARTESIAN_POINT('Ctrl Pts',(117.905484322383,-2.11686731366726,330.558719447037));
#55273=CARTESIAN_POINT('Ctrl Pts',(117.898072518206,-2.2327578765785,330.617765943371));
#55274=CARTESIAN_POINT('Ctrl Pts',(117.890297439428,-2.35432858119775,330.679706484381));
#55275=CARTESIAN_POINT('Ctrl Pts',(117.882522360649,-2.47351193234357,330.746807606973));
#55276=CARTESIAN_POINT('Ctrl Pts',(117.874747281871,-2.58983888197942,330.818861682761));
#55277=CARTESIAN_POINT('Ctrl Pts',(117.866981770822,-2.706022683898,330.890827091421));
#55278=CARTESIAN_POINT('Ctrl Pts',(117.859216259773,-2.81935674900042,330.967733122267));
#55279=CARTESIAN_POINT('Ctrl Pts',(117.851450748724,-2.92939451705489,331.049325269533));
#55280=CARTESIAN_POINT('Ctrl Pts',(117.843692937201,-3.03932318234206,331.130836517948));
#55281=CARTESIAN_POINT('Ctrl Pts',(117.835935125679,-3.14596174270503,331.217024405074));
#55282=CARTESIAN_POINT('Ctrl Pts',(117.828177314157,-3.24889096056355,331.307590138017));
#55283=CARTESIAN_POINT('Ctrl Pts',(117.820425340634,-3.3517427209215,331.398087717375));
#55284=CARTESIAN_POINT('Ctrl Pts',(117.812673367111,-3.45089040264602,331.492956327909));
#55285=CARTESIAN_POINT('Ctrl Pts',(117.804921393588,-3.54594662000991,331.591855984478));
#55286=CARTESIAN_POINT('Ctrl Pts',(117.79717270303,-3.64096258100934,331.690713756983));
#55287=CARTESIAN_POINT('Ctrl Pts',(117.789424012473,-3.73189025364509,331.793598898897));
#55288=CARTESIAN_POINT('Ctrl Pts',(117.781675321915,-3.81837818158028,331.90013369241));
#55289=CARTESIAN_POINT('Ctrl Pts',(117.773928243537,-3.90484811497968,332.00664632047));
#55290=CARTESIAN_POINT('Ctrl Pts',(117.766181165159,-3.9868798948299,332.116806786475));
#55291=CARTESIAN_POINT('Ctrl Pts',(117.758434086782,-4.06416180535297,332.230203638819));
#55292=CARTESIAN_POINT('Ctrl Pts',(117.750686943476,-4.14144436357289,332.343601441538));
#55293=CARTESIAN_POINT('Ctrl Pts',(117.74293980017,-4.21397675293714,332.460235361701));
#55294=CARTESIAN_POINT('Ctrl Pts',(117.735192656864,-4.28149035151387,332.579664603326));
#55295=CARTESIAN_POINT('Ctrl Pts',(117.727443771836,-4.34901912858079,332.699120695179));
#55296=CARTESIAN_POINT('Ctrl Pts',(117.719694886808,-4.41152667729135,332.821373018834));
#55297=CARTESIAN_POINT('Ctrl Pts',(117.71194600178,-4.46879032565175,332.945956162137));
#55298=CARTESIAN_POINT('Ctrl Pts',(117.704188892005,-4.52611475424024,333.070671539277));
#55299=CARTESIAN_POINT('Ctrl Pts',(117.69643178223,-4.57818400050974,333.19772232231));
#55300=CARTESIAN_POINT('Ctrl Pts',(117.688674672456,-4.62482335785744,333.326622585572));
#55301=CARTESIAN_POINT('Ctrl Pts',(117.680913417529,-4.67148763778646,333.455591729014));
#55302=CARTESIAN_POINT('Ctrl Pts',(117.673152162603,-4.71271612974655,333.586411949358));
#55303=CARTESIAN_POINT('Ctrl Pts',(117.665390907677,-4.74838433486586,333.718583100275));
#55304=CARTESIAN_POINT('Ctrl Pts',(117.657617237272,-4.78410959748912,333.850965681959));
#55305=CARTESIAN_POINT('Ctrl Pts',(117.649843566868,-4.81425671313375,333.984703131125));
#55306=CARTESIAN_POINT('Ctrl Pts',(117.642069896463,-4.83875236983975,334.119285196065));
#55307=CARTESIAN_POINT('Ctrl Pts',(117.634658092286,-4.86210774783247,334.247602433502));
#55308=CARTESIAN_POINT('Ctrl Pts',(117.627246288109,-4.88032593679839,334.376687137616));
#55309=CARTESIAN_POINT('Ctrl Pts',(117.619834483932,-4.89338751171919,334.506095431636));
#55310=CARTESIAN_POINT('Ctrl Pts',(117.610495448124,-4.90984538256678,334.669152720096));
#55311=CARTESIAN_POINT('Ctrl Pts',(117.601156412316,-4.91815503121431,334.833046133824));
#55312=CARTESIAN_POINT('Ctrl Pts',(117.591817376508,-4.91824919068047,334.997178498468));
#55313=CARTESIAN_POINT('',(115.84181737656,-4.91824921532725,334.997221793222));
#55314=CARTESIAN_POINT('Ctrl Pts',(117.59181737647,-4.91824919068085,334.99717849913));
#55315=CARTESIAN_POINT('Ctrl Pts',(117.584144529207,-4.91832655102595,335.132027812359));
#55316=CARTESIAN_POINT('Ctrl Pts',(117.576471681944,-4.91285375398507,335.267100332213));
#55317=CARTESIAN_POINT('Ctrl Pts',(117.56879883468,-4.90180212690904,335.401894228784));
#55318=CARTESIAN_POINT('Ctrl Pts',(117.561134564802,-4.89076285431585,335.536537440856));
#55319=CARTESIAN_POINT('Ctrl Pts',(117.553470294923,-4.87415718779738,335.670902252343));
#55320=CARTESIAN_POINT('Ctrl Pts',(117.545806025045,-4.85200845814346,335.804485540333));
#55321=CARTESIAN_POINT('Ctrl Pts',(117.538148379225,-4.82987887114447,335.937953375255));
#55322=CARTESIAN_POINT('Ctrl Pts',(117.530490733404,-4.80221581649998,336.070640636286));
#55323=CARTESIAN_POINT('Ctrl Pts',(117.522833087584,-4.76909450283843,336.20204853708));
#55324=CARTESIAN_POINT('Ctrl Pts',(117.515179689865,-4.7359915633218,336.333383538959));
#55325=CARTESIAN_POINT('Ctrl Pts',(117.507526292146,-4.69743648457715,336.463440203752));
#55326=CARTESIAN_POINT('Ctrl Pts',(117.499872894427,-4.65355562973359,336.591729582396));
#55327=CARTESIAN_POINT('Ctrl Pts',(117.492221660361,-4.6096871802239,336.719982693001));
#55328=CARTESIAN_POINT('Ctrl Pts',(117.484570426295,-4.5604960777282,336.846469131093));
#55329=CARTESIAN_POINT('Ctrl Pts',(117.476919192229,-4.50615851227743,336.97071523177));
#55330=CARTESIAN_POINT('Ctrl Pts',(117.469268366191,-4.45182384456133,337.094954706603));
#55331=CARTESIAN_POINT('Ctrl Pts',(117.461617540154,-4.39234342062797,337.216953713654));
#55332=CARTESIAN_POINT('Ctrl Pts',(117.453966714116,-4.32794131306079,337.336259200774));
#55333=CARTESIAN_POINT('Ctrl Pts',(117.446314541037,-4.26352786655405,337.455585693383));
#55334=CARTESIAN_POINT('Ctrl Pts',(117.438662367959,-4.1941912043012,337.572217369784));
#55335=CARTESIAN_POINT('Ctrl Pts',(117.43101019488,-4.12020075350308,337.685726868714));
#55336=CARTESIAN_POINT('Ctrl Pts',(117.42335028893,-4.04613553196235,337.799351074197));
#55337=CARTESIAN_POINT('Ctrl Pts',(117.41569038298,-3.96740734910642,337.909846463974));
#55338=CARTESIAN_POINT('Ctrl Pts',(117.40803047703,-3.88432848554171,338.016815420093));
#55339=CARTESIAN_POINT('Ctrl Pts',(117.400366632117,-3.8012069002403,338.123839382977));
#55340=CARTESIAN_POINT('Ctrl Pts',(117.392702787205,-3.71373043828124,338.227332994806));
#55341=CARTESIAN_POINT('Ctrl Pts',(117.385038942293,-3.62225002662831,338.326933694424));
#55342=CARTESIAN_POINT('Ctrl Pts',(117.37736309491,-3.53062634603469,338.426690380295));
#55343=CARTESIAN_POINT('Ctrl Pts',(117.369687247528,-3.43498647310173,338.522541691041));
#55344=CARTESIAN_POINT('Ctrl Pts',(117.362011400145,-3.33571684786384,338.614163274311));
#55345=CARTESIAN_POINT('Ctrl Pts',(117.355206416649,-3.24770986600406,338.695389923424));
#55346=CARTESIAN_POINT('Ctrl Pts',(117.348401433154,-3.15685067194417,338.773292636824));
#55347=CARTESIAN_POINT('Ctrl Pts',(117.341596449658,-3.06342765363515,338.84767385227));
#55348=CARTESIAN_POINT('Ctrl Pts',(117.333821370879,-2.95668656785087,338.932658600595));
#55349=CARTESIAN_POINT('Ctrl Pts',(117.326046292101,-2.84623769652375,339.013332503847));
#55350=CARTESIAN_POINT('Ctrl Pts',(117.318271213323,-2.73246433625197,339.089354681806));
#55351=CARTESIAN_POINT('Ctrl Pts',(117.310505702274,-2.61883098134325,339.165283309636));
#55352=CARTESIAN_POINT('Ctrl Pts',(117.302740191225,-2.50188159928907,339.236571386691));
#55353=CARTESIAN_POINT('Ctrl Pts',(117.294974680176,-2.38203283510247,339.302917921015));
#55354=CARTESIAN_POINT('Ctrl Pts',(117.287216868653,-2.2623029013147,339.369198672557));
#55355=CARTESIAN_POINT('Ctrl Pts',(117.279459057131,-2.13967964606959,339.430547443665));
#55356=CARTESIAN_POINT('Ctrl Pts',(117.271701245609,-2.0146087022326,339.486706457903));
#55357=CARTESIAN_POINT('Ctrl Pts',(117.263949272086,-1.88963187824648,339.542823210702));
#55358=CARTESIAN_POINT('Ctrl Pts',(117.256197298563,-1.76221138714826,339.593757820786));
#55359=CARTESIAN_POINT('Ctrl Pts',(117.24844532504,-1.63281715644165,339.639298567255));
#55360=CARTESIAN_POINT('Ctrl Pts',(117.240696634482,-1.50347772426891,339.68482002719));
#55361=CARTESIAN_POINT('Ctrl Pts',(117.232947943925,-1.3721665829315,339.724952037333));
#55362=CARTESIAN_POINT('Ctrl Pts',(117.225199253367,-1.23937311654837,339.759531210159));
#55363=CARTESIAN_POINT('Ctrl Pts',(117.217452174989,-1.10660727895499,339.7941031885));
#55364=CARTESIAN_POINT('Ctrl Pts',(117.209705096611,-0.972360107788149,
339.823124529089));
#55365=CARTESIAN_POINT('Ctrl Pts',(117.201958018233,-0.837135225290063,
339.846481989761));
#55366=CARTESIAN_POINT('Ctrl Pts',(117.194210874928,-0.701909209477538,
339.869839646191));
#55367=CARTESIAN_POINT('Ctrl Pts',(117.186463731622,-0.565705851160481,
339.887533261494));
#55368=CARTESIAN_POINT('Ctrl Pts',(117.178716588316,-0.429037626449165,
339.899500972302));
#55369=CARTESIAN_POINT('Ctrl Pts',(117.170967703288,-0.292338675819384,
339.911471373706));
#55370=CARTESIAN_POINT('Ctrl Pts',(117.16321881826,-0.155175040136601,339.917713274931));
#55371=CARTESIAN_POINT('Ctrl Pts',(117.155469933232,-0.0180625627713276,
339.918216831975));
#55372=CARTESIAN_POINT('Ctrl Pts',(117.147712823457,0.119195447194198,339.9187209235));
#55373=CARTESIAN_POINT('Ctrl Pts',(117.139955713682,0.256401798883917,339.913474502585));
#55374=CARTESIAN_POINT('Ctrl Pts',(117.132198603908,0.393041850661492,339.902519879218));
#55375=CARTESIAN_POINT('Ctrl Pts',(117.124437348981,0.529754918513928,339.891559402051));
#55376=CARTESIAN_POINT('Ctrl Pts',(117.116676094055,0.66590069569305,339.874884691966));
#55377=CARTESIAN_POINT('Ctrl Pts',(117.108914839129,0.800972398676446,339.852589646679));
#55378=CARTESIAN_POINT('Ctrl Pts',(117.101141168724,0.936260172364942,339.830258936586));
#55379=CARTESIAN_POINT('Ctrl Pts',(117.09336749832,1.07047005559319,339.802290004985));
#55380=CARTESIAN_POINT('Ctrl Pts',(117.085593827915,1.20310727411774,339.76882752356));
#55381=CARTESIAN_POINT('Ctrl Pts',(117.078182023738,1.32957019820814,339.736922728697));
#55382=CARTESIAN_POINT('Ctrl Pts',(117.070770219561,1.45460330167092,339.700024405104));
#55383=CARTESIAN_POINT('Ctrl Pts',(117.063358415384,1.57779454607045,339.658298770248));
#55384=CARTESIAN_POINT('Ctrl Pts',(117.055583336606,1.70702376032662,339.614528037733));
#55385=CARTESIAN_POINT('Ctrl Pts',(117.047808257827,1.83463438850358,339.565306503628));
#55386=CARTESIAN_POINT('Ctrl Pts',(117.040033179049,1.96013235336833,339.510772020373));
#55387=CARTESIAN_POINT('Ctrl Pts',(117.032267668,2.08547588499781,339.456304645271));
#55388=CARTESIAN_POINT('Ctrl Pts',(117.024502156951,2.20871157104214,339.3965374839));
#55389=CARTESIAN_POINT('Ctrl Pts',(117.016736645902,2.32936083041821,339.33165801792));
#55390=CARTESIAN_POINT('Ctrl Pts',(117.008978834379,2.44989046570219,339.26684288012));
#55391=CARTESIAN_POINT('Ctrl Pts',(117.001221022857,2.56783843567985,339.196925708971));
#55392=CARTESIAN_POINT('Ctrl Pts',(116.993463211335,2.68274681313196,339.122141749034));
#55393=CARTESIAN_POINT('Ctrl Pts',(116.985711237812,2.79756871838577,339.047414066399));
#55394=CARTESIAN_POINT('Ctrl Pts',(116.977959264289,2.90935525776649,338.967827097182));
#55395=CARTESIAN_POINT('Ctrl Pts',(116.970207290766,3.01767408591497,338.883661439119));
#55396=CARTESIAN_POINT('Ctrl Pts',(116.962458600209,3.12594704097579,338.799531425261));
#55397=CARTESIAN_POINT('Ctrl Pts',(116.954709909651,3.23075489769328,338.710826818573));
#55398=CARTESIAN_POINT('Ctrl Pts',(116.946961219093,3.33169542618465,338.617870734236));
#55399=CARTESIAN_POINT('Ctrl Pts',(116.939214140716,3.43261495315607,338.524933990189));
#55400=CARTESIAN_POINT('Ctrl Pts',(116.931467062338,3.52966846502012,338.427747792554));
#55401=CARTESIAN_POINT('Ctrl Pts',(116.92371998396,3.62248819513091,338.326674366186));
#55402=CARTESIAN_POINT('Ctrl Pts',(116.915972840654,3.7153087031605,338.225600092725));
#55403=CARTESIAN_POINT('Ctrl Pts',(116.908225697348,3.80389509427798,338.120638813444));
#55404=CARTESIAN_POINT('Ctrl Pts',(116.900478554042,3.88791801602921,338.012188002621));
#55405=CARTESIAN_POINT('Ctrl Pts',(116.892729669014,3.97195982791705,337.903712809753));
#55406=CARTESIAN_POINT('Ctrl Pts',(116.884980783986,4.05143588953866,337.791746833163));
#55407=CARTESIAN_POINT('Ctrl Pts',(116.877231898958,4.12605877041466,337.676718529391));
#55408=CARTESIAN_POINT('Ctrl Pts',(116.869474789183,4.20076085678731,337.561568133389));
#55409=CARTESIAN_POINT('Ctrl Pts',(116.861717679409,4.27059925931053,337.443349245687));
#55410=CARTESIAN_POINT('Ctrl Pts',(116.853960569634,4.33533105523617,337.32251753578));
#55411=CARTESIAN_POINT('Ctrl Pts',(116.846199314708,4.40009744176379,337.20162125727));
#55412=CARTESIAN_POINT('Ctrl Pts',(116.838438059782,4.45975161438901,337.078109726277));
#55413=CARTESIAN_POINT('Ctrl Pts',(116.830676804855,4.51409828406028,336.952459921316));
#55414=CARTESIAN_POINT('Ctrl Pts',(116.822903134451,4.56853189069155,336.826609117616));
#55415=CARTESIAN_POINT('Ctrl Pts',(116.815129464046,4.61764088819396,336.698613569821));
#55416=CARTESIAN_POINT('Ctrl Pts',(116.807355793642,4.66127918333878,336.568967634297));
#55417=CARTESIAN_POINT('Ctrl Pts',(116.799943989464,4.70288610534631,336.445356748262));
#55418=CARTESIAN_POINT('Ctrl Pts',(116.792532185287,4.73952010452823,336.320245943972));
#55419=CARTESIAN_POINT('Ctrl Pts',(116.78512038111,4.77109797905778,336.194071663147));
#55420=CARTESIAN_POINT('Ctrl Pts',(116.777345302332,4.8042235792833,336.061713204967));
#55421=CARTESIAN_POINT('Ctrl Pts',(116.769570223553,4.83188957436215,335.927766108844));
#55422=CARTESIAN_POINT('Ctrl Pts',(116.761795144775,4.85394451381067,335.79272045473));
#55423=CARTESIAN_POINT('Ctrl Pts',(116.754029633726,4.87597231325211,335.657840982891));
#55424=CARTESIAN_POINT('Ctrl Pts',(116.746264122677,4.89240273315953,335.521866024921));
#55425=CARTESIAN_POINT('Ctrl Pts',(116.738498611628,4.90313444317588,335.385299486948));
#55426=CARTESIAN_POINT('Ctrl Pts',(116.730740800105,4.91385551267051,335.248868355095));
#55427=CARTESIAN_POINT('Ctrl Pts',(116.722982988583,4.91888908624141,335.111847197675));
#55428=CARTESIAN_POINT('Ctrl Pts',(116.715225177061,4.91818517536568,334.974748399788));
#55429=CARTESIAN_POINT('Ctrl Pts',(116.707473203538,4.91748179420521,334.837752773094));
#55430=CARTESIAN_POINT('Ctrl Pts',(116.699721230015,4.91104952464625,334.700680011525));
#55431=CARTESIAN_POINT('Ctrl Pts',(116.691969256492,4.89889036042889,334.564045531051));
#55432=CARTESIAN_POINT('Ctrl Pts',(116.684220565934,4.88673634562477,334.42746891536));
#55433=CARTESIAN_POINT('Ctrl Pts',(116.676471875377,4.86886029457421,334.29133060012));
#55434=CARTESIAN_POINT('Ctrl Pts',(116.668723184819,4.84531625205711,334.156143685186));
#55435=CARTESIAN_POINT('Ctrl Pts',(116.660976106441,4.82177710807469,334.020984897019));
#55436=CARTESIAN_POINT('Ctrl Pts',(116.653229028063,4.7925723853058,333.886777500263));
#55437=CARTESIAN_POINT('Ctrl Pts',(116.645481949686,4.75780766672358,333.754026778391));
#55438=CARTESIAN_POINT('Ctrl Pts',(116.63773480638,4.7230426567796,333.62127494394));
#55439=CARTESIAN_POINT('Ctrl Pts',(116.629987663074,4.68271765710167,333.489980186847));
#55440=CARTESIAN_POINT('Ctrl Pts',(116.622240519768,4.63698868077768,333.360634562753));
#55441=CARTESIAN_POINT('Ctrl Pts',(116.61449163474,4.59124942360894,333.231259859017));
#55442=CARTESIAN_POINT('Ctrl Pts',(116.606742749712,4.54010390248369,333.103835528713));
#55443=CARTESIAN_POINT('Ctrl Pts',(116.598993864684,4.48375687052214,332.978835140681));
#55444=CARTESIAN_POINT('Ctrl Pts',(116.591236754909,4.42735003123865,332.853702075946));
#55445=CARTESIAN_POINT('Ctrl Pts',(116.583479645134,4.36573081341286,332.730998449793));
#55446=CARTESIAN_POINT('Ctrl Pts',(116.57572253536,4.29915093980522,332.611175130054));
#55447=CARTESIAN_POINT('Ctrl Pts',(116.567961280433,4.23253548804204,332.491287780564));
#55448=CARTESIAN_POINT('Ctrl Pts',(116.560200025507,4.16095430238943,332.374284137627));
#55449=CARTESIAN_POINT('Ctrl Pts',(116.552438770581,4.08470280214685,332.260586544416));
#55450=CARTESIAN_POINT('Ctrl Pts',(116.544665100176,4.00832932435404,332.14670707211));
#55451=CARTESIAN_POINT('Ctrl Pts',(116.536891429772,3.92727083397016,332.036144533121));
#55452=CARTESIAN_POINT('Ctrl Pts',(116.529117759367,3.84186398638091,331.929289304957));
#55453=CARTESIAN_POINT('Ctrl Pts',(116.52170595519,3.76043284809528,331.827408213373));
#55454=CARTESIAN_POINT('Ctrl Pts',(116.514294151013,3.67504926266306,331.728897266853));
#55455=CARTESIAN_POINT('Ctrl Pts',(116.506882346836,3.58603521795476,331.634062615245));
#55456=CARTESIAN_POINT('Ctrl Pts',(116.499107268058,3.49265832975548,331.534579834864));
#55457=CARTESIAN_POINT('Ctrl Pts',(116.491332189279,3.39499101640154,331.438828449779));
#55458=CARTESIAN_POINT('Ctrl Pts',(116.483557110501,3.29336343803204,331.347201028316));
#55459=CARTESIAN_POINT('Ctrl Pts',(116.475791599452,3.1918609188678,331.255686360229));
#55460=CARTESIAN_POINT('Ctrl Pts',(116.468026088403,3.08640811880186,331.168285817602));
#55461=CARTESIAN_POINT('Ctrl Pts',(116.460260577354,2.97737394757625,331.085357303815));
#55462=CARTESIAN_POINT('Ctrl Pts',(116.452502765831,2.8684478840493,331.002511013891));
#55463=CARTESIAN_POINT('Ctrl Pts',(116.444744954309,2.75594782504317,330.924128163937));
#55464=CARTESIAN_POINT('Ctrl Pts',(116.436987142787,2.64027759446093,330.850528071346));
#55465=CARTESIAN_POINT('Ctrl Pts',(116.429235169264,2.52469440939517,330.776983365159));
#55466=CARTESIAN_POINT('Ctrl Pts',(116.421483195741,2.40594612973061,330.708214461339));
#55467=CARTESIAN_POINT('Ctrl Pts',(116.413731222218,2.2844672586807,330.644498604464));
#55468=CARTESIAN_POINT('Ctrl Pts',(116.405982531661,2.16303983400456,330.580809731293));
#55469=CARTESIAN_POINT('Ctrl Pts',(116.398233841103,2.0388844633851,330.522169829999));
#55470=CARTESIAN_POINT('Ctrl Pts',(116.390485150545,1.91246187016815,330.468811120947));
#55471=CARTESIAN_POINT('Ctrl Pts',(116.382738072168,1.78606558022753,330.415463513621));
#55472=CARTESIAN_POINT('Ctrl Pts',(116.37499099379,1.65740336584989,330.367395064849));
#55473=CARTESIAN_POINT('Ctrl Pts',(116.367243915412,1.52695726769135,330.324790425538));
#55474=CARTESIAN_POINT('Ctrl Pts',(116.359496772106,1.39651007626887,330.282185429158));
#55475=CARTESIAN_POINT('Ctrl Pts',(116.3517496288,1.26427934280408,330.245044454928));
#55476=CARTESIAN_POINT('Ctrl Pts',(116.344002485494,1.13076327501897,330.213502587657));
#55477=CARTESIAN_POINT('Ctrl Pts',(116.336253600466,0.997217189986916,330.181953629104));
#55478=CARTESIAN_POINT('Ctrl Pts',(116.328504715438,0.862385575944641,330.156006372225));
#55479=CARTESIAN_POINT('Ctrl Pts',(116.32075583041,0.726777470695663,330.135744911028));
#55480=CARTESIAN_POINT('Ctrl Pts',(116.312998720635,0.59102542960305,330.115461944107));
#55481=CARTESIAN_POINT('Ctrl Pts',(116.305241610861,0.454495638128982,330.100876886121));
#55482=CARTESIAN_POINT('Ctrl Pts',(116.297484501086,0.317703462280664,330.092022048485));
#55483=CARTESIAN_POINT('Ctrl Pts',(116.28972324616,0.180838189067712,330.083162479108));
#55484=CARTESIAN_POINT('Ctrl Pts',(116.281961991234,0.043710642674533,330.080039240379));
#55485=CARTESIAN_POINT('Ctrl Pts',(116.274200736308,-0.0931641511791335,
330.082632462035));
#55486=CARTESIAN_POINT('Ctrl Pts',(116.266427065903,-0.230257900095948,
330.085229832));
#55487=CARTESIAN_POINT('Ctrl Pts',(116.258653395498,-0.367097698161858,
330.093561911946));
#55488=CARTESIAN_POINT('Ctrl Pts',(116.250879725094,-0.503173085055177,
330.107556856848));
#55489=CARTESIAN_POINT('Ctrl Pts',(116.243467920916,-0.632914129952058,
330.120900333698));
#55490=CARTESIAN_POINT('Ctrl Pts',(116.236056116739,-0.761960043908237,
330.139391286548));
#55491=CARTESIAN_POINT('Ctrl Pts',(116.228644312562,-0.889879132872186,
330.162924624179));
#55492=CARTESIAN_POINT('Ctrl Pts',(116.220869233784,-1.02406791743659,330.187611400789));
#55493=CARTESIAN_POINT('Ctrl Pts',(116.213094155005,-1.15744068732577,330.217925359546));
#55494=CARTESIAN_POINT('Ctrl Pts',(116.205319076227,-1.28948865486437,330.253801302992));
#55495=CARTESIAN_POINT('Ctrl Pts',(116.197553565178,-1.4213741289716,330.289633098806));
#55496=CARTESIAN_POINT('Ctrl Pts',(116.189788054129,-1.55193767087079,330.331013159461));
#55497=CARTESIAN_POINT('Ctrl Pts',(116.18202254308,-1.68067867374598,330.377824942939));
#55498=CARTESIAN_POINT('Ctrl Pts',(116.174264731558,-1.80929202954278,330.424590312398));
#55499=CARTESIAN_POINT('Ctrl Pts',(116.166506920035,-1.9360860774751,330.476776554383));
#55500=CARTESIAN_POINT('Ctrl Pts',(116.158749108513,-2.0605737644493,330.534216885723));
#55501=CARTESIAN_POINT('Ctrl Pts',(116.15099713499,-2.18496777049114,330.591613991392));
#55502=CARTESIAN_POINT('Ctrl Pts',(116.143245161467,-2.3070585167355,330.65425715333));
#55503=CARTESIAN_POINT('Ctrl Pts',(116.135493187944,-2.42637772768128,330.721931021464));
#55504=CARTESIAN_POINT('Ctrl Pts',(116.127744497387,-2.54564640687014,330.789576229675));
#55505=CARTESIAN_POINT('Ctrl Pts',(116.119995806829,-2.66214554597141,330.862247714221));
#55506=CARTESIAN_POINT('Ctrl Pts',(116.112247116271,-2.77543054208758,330.939683710775));
#55507=CARTESIAN_POINT('Ctrl Pts',(116.104500037894,-2.88869196831414,331.017103596123));
#55508=CARTESIAN_POINT('Ctrl Pts',(116.096752959516,-2.99874025921742,331.099285801284));
#55509=CARTESIAN_POINT('Ctrl Pts',(116.089005881138,-3.10515927805352,331.185924893186));
#55510=CARTESIAN_POINT('Ctrl Pts',(116.081258737832,-3.21157918878343,331.272564711207));
#55511=CARTESIAN_POINT('Ctrl Pts',(116.073511594526,-3.31436946365678,331.363661243692));
#55512=CARTESIAN_POINT('Ctrl Pts',(116.065764451221,-3.41314689819048,331.45886863928));
#55513=CARTESIAN_POINT('Ctrl Pts',(116.058015566193,-3.51194653998911,331.554097439513));
#55514=CARTESIAN_POINT('Ctrl Pts',(116.050266681164,-3.60673126485332,331.653438670718));
#55515=CARTESIAN_POINT('Ctrl Pts',(116.042517796136,-3.69715488677519,331.756509780238));
#55516=CARTESIAN_POINT('Ctrl Pts',(116.034760686362,-3.78767448526299,331.859690290497));
#55517=CARTESIAN_POINT('Ctrl Pts',(116.027003576587,-3.87382347592597,331.966608293117));
#55518=CARTESIAN_POINT('Ctrl Pts',(116.019246466812,-3.95529579328814,332.076847891386));
#55519=CARTESIAN_POINT('Ctrl Pts',(116.011485211886,-4.03681164685179,332.187146398171));
#55520=CARTESIAN_POINT('Ctrl Pts',(116.00372395696,-4.11364562866012,332.300769713734));
#55521=CARTESIAN_POINT('Ctrl Pts',(115.995962702034,-4.18553573807435,332.417273989018));
#55522=CARTESIAN_POINT('Ctrl Pts',(115.988189031629,-4.25754084823477,332.533964633174));
#55523=CARTESIAN_POINT('Ctrl Pts',(115.980415361224,-4.32458609104988,332.653545105271));
#55524=CARTESIAN_POINT('Ctrl Pts',(115.97264169082,-4.38645564316487,332.775547268867));
#55525=CARTESIAN_POINT('Ctrl Pts',(115.965229886643,-4.44544515274365,332.891870202394));
#55526=CARTESIAN_POINT('Ctrl Pts',(115.957818082466,-4.49972986469864,333.01039418011));
#55527=CARTESIAN_POINT('Ctrl Pts',(115.950406278289,-4.54916453805657,333.130699310387));
#55528=CARTESIAN_POINT('Ctrl Pts',(115.941357203145,-4.60951935359828,333.277579899523));
#55529=CARTESIAN_POINT('Ctrl Pts',(115.932308128001,-4.66281245506729,333.42752295293));
#55530=CARTESIAN_POINT('Ctrl Pts',(115.923259052857,-4.70875950389444,333.579870781589));
#55531=CARTESIAN_POINT('Ctrl Pts',(115.914584544033,-4.75280467692059,333.725912511031));
#55532=CARTESIAN_POINT('Ctrl Pts',(115.90591003521,-4.79009954401527,333.874163693861));
#55533=CARTESIAN_POINT('Ctrl Pts',(115.897235526387,-4.82044076125398,334.024021552625));
#55534=CARTESIAN_POINT('Ctrl Pts',(115.888587993326,-4.85068762416624,334.173413387326));
#55535=CARTESIAN_POINT('Ctrl Pts',(115.879940460264,-4.87402390341494,334.324401719336));
#55536=CARTESIAN_POINT('Ctrl Pts',(115.871292927202,-4.89029591783363,334.47636950192));
#55537=CARTESIAN_POINT('Ctrl Pts',(115.86268627168,-4.90649101321472,334.627618921351));
#55538=CARTESIAN_POINT('Ctrl Pts',(115.854079616159,-4.91568837694199,334.77983833998));
#55539=CARTESIAN_POINT('Ctrl Pts',(115.845472960637,-4.9177854448456,334.932402803573));
#55540=CARTESIAN_POINT('Ctrl Pts',(115.844254432611,-4.91808234716799,334.954002840213));
#55541=CARTESIAN_POINT('Ctrl Pts',(115.843035904585,-4.91823700718782,334.975609769017));
#55542=CARTESIAN_POINT('Ctrl Pts',(115.84181737656,-4.91824921532725,334.997221793222));
#55543=CARTESIAN_POINT('',(114.09181737646,-4.91824836605016,335.004009032921));
#55544=CARTESIAN_POINT('Ctrl Pts',(115.841817376508,-4.91824921532777,334.997221794137));
#55545=CARTESIAN_POINT('Ctrl Pts',(115.833984682288,-4.91832768918275,335.136143816042));
#55546=CARTESIAN_POINT('Ctrl Pts',(115.826151988068,-4.91251578406707,335.275072939698));
#55547=CARTESIAN_POINT('Ctrl Pts',(115.818319293848,-4.90083827818156,335.413481841935));
#55548=CARTESIAN_POINT('Ctrl Pts',(115.810485101013,-4.88915853806036,335.551917225693));
#55549=CARTESIAN_POINT('Ctrl Pts',(115.802650908177,-4.8716109934746,335.689831812301));
#55550=CARTESIAN_POINT('Ctrl Pts',(115.794816715342,-4.84827231816433,335.826703448294));
#55551=CARTESIAN_POINT('Ctrl Pts',(115.786979472975,-4.82492455805909,335.963628362836));
#55552=CARTESIAN_POINT('Ctrl Pts',(115.779142230608,-4.79578124125216,336.099509144996));
#55553=CARTESIAN_POINT('Ctrl Pts',(115.771304988241,-4.76097011595331,336.233834112634));
#55554=CARTESIAN_POINT('Ctrl Pts',(115.763463143711,-4.72613854896433,336.368237958198));
#55555=CARTESIAN_POINT('Ctrl Pts',(115.755621299181,-4.68563263977677,336.501083803625));
#55556=CARTESIAN_POINT('Ctrl Pts',(115.74777945465,-4.63962983588254,336.631875622861));
#55557=CARTESIAN_POINT('Ctrl Pts',(115.739926779051,-4.59356349342512,336.76284809031));
#55558=CARTESIAN_POINT('Ctrl Pts',(115.732074103452,-4.5419852213524,336.891760509309));
#55559=CARTESIAN_POINT('Ctrl Pts',(115.724221427853,-4.48512066900968,337.018136676968));
#55560=CARTESIAN_POINT('Ctrl Pts',(115.716362315279,-4.42820950379904,337.144616437381));
#55561=CARTESIAN_POINT('Ctrl Pts',(115.708503202704,-4.36600359200974,337.268555466074));
#55562=CARTESIAN_POINT('Ctrl Pts',(115.70064409013,-4.2987739076315,337.38950328595));
#55563=CARTESIAN_POINT('Ctrl Pts',(115.692772760256,-4.23143971206717,337.510639123965));
#55564=CARTESIAN_POINT('Ctrl Pts',(115.684901430382,-4.15906634776463,337.628774147442));
#55565=CARTESIAN_POINT('Ctrl Pts',(115.677030100508,-4.0819676517212,337.743487407079));
#55566=CARTESIAN_POINT('Ctrl Pts',(115.675409481677,-4.06609389205533,337.767105584914));
#55567=CARTESIAN_POINT('Ctrl Pts',(115.673788862845,-4.05001995799648,337.790578828913));
#55568=CARTESIAN_POINT('Ctrl Pts',(115.672168244014,-4.03374879222463,337.813903648622));
#55569=CARTESIAN_POINT('Ctrl Pts',(115.664393165236,-3.95568626866411,337.925806773053));
#55570=CARTESIAN_POINT('Ctrl Pts',(115.656618086457,-3.87284028544115,338.034635881784));
#55571=CARTESIAN_POINT('Ctrl Pts',(115.648843007679,-3.78548097087406,338.139954917137));
#55572=CARTESIAN_POINT('Ctrl Pts',(115.64107749663,-3.69822915750517,338.245144350711));
#55573=CARTESIAN_POINT('Ctrl Pts',(115.633311985581,-3.60647531070338,338.346832007239));
#55574=CARTESIAN_POINT('Ctrl Pts',(115.625546474532,-3.51053290029633,338.4446105467));
#55575=CARTESIAN_POINT('Ctrl Pts',(115.61778866301,-3.41468561706853,338.542292138454));
#55576=CARTESIAN_POINT('Ctrl Pts',(115.610030851487,-3.31465830688097,338.636072049203));
#55577=CARTESIAN_POINT('Ctrl Pts',(115.602273039965,-3.21080455085213,338.72557608951));
#55578=CARTESIAN_POINT('Ctrl Pts',(115.594521066442,-3.1070289480681,338.815012775188));
#55579=CARTESIAN_POINT('Ctrl Pts',(115.586769092919,-2.99943292588546,338.900179741005));
#55580=CARTESIAN_POINT('Ctrl Pts',(115.579017119396,-2.88840648867091,338.980740008931));
#55581=CARTESIAN_POINT('Ctrl Pts',(115.571268428839,-2.77742707121852,339.061266159536));
#55582=CARTESIAN_POINT('Ctrl Pts',(115.563519738281,-2.66302044392482,339.137189263455));
#55583=CARTESIAN_POINT('Ctrl Pts',(115.555771047723,-2.54560904720101,339.208213117382));
#55584=CARTESIAN_POINT('Ctrl Pts',(115.548023969346,-2.42822207889877,339.279222194204));
#55585=CARTESIAN_POINT('Ctrl Pts',(115.540276890968,-2.30783191890321,339.34533384637));
#55586=CARTESIAN_POINT('Ctrl Pts',(115.53252981259,-2.18488895891302,339.406295870651));
#55587=CARTESIAN_POINT('Ctrl Pts',(115.524782669284,-2.06194496854258,339.467258405853));
#55588=CARTESIAN_POINT('Ctrl Pts',(115.517035525978,-1.93644848569086,339.523071053445));
#55589=CARTESIAN_POINT('Ctrl Pts',(115.509288382672,-1.8088730446726,339.573528328409));
#55590=CARTESIAN_POINT('Ctrl Pts',(115.501539497644,-1.68126892198678,339.623996947239));
#55591=CARTESIAN_POINT('Ctrl Pts',(115.493790612616,-1.55158527447946,339.669107653882));
#55592=CARTESIAN_POINT('Ctrl Pts',(115.486041727588,-1.42031370318315,339.708703860623));
#55593=CARTESIAN_POINT('Ctrl Pts',(115.478284617813,-1.28890279888477,339.748342095188));
#55594=CARTESIAN_POINT('Ctrl Pts',(115.470527508039,-1.15590097878726,339.782454024584));
#55595=CARTESIAN_POINT('Ctrl Pts',(115.462770398264,-1.0218135699008,339.810933390816));
#55596=CARTESIAN_POINT('Ctrl Pts',(115.455009143338,-0.887654508990122,
339.83942797551));
#55597=CARTESIAN_POINT('Ctrl Pts',(115.447247888412,-0.752409088595061,
339.86228393452));
#55598=CARTESIAN_POINT('Ctrl Pts',(115.439486633486,-0.616589820371562,
339.879446695673));
#55599=CARTESIAN_POINT('Ctrl Pts',(115.431712963081,-0.480553285582395,
339.896636911651));
#55600=CARTESIAN_POINT('Ctrl Pts',(115.423939292676,-0.343941458296462,
339.908115698022));
#55601=CARTESIAN_POINT('Ctrl Pts',(115.416165622272,-0.207269824000443,
339.91388057268));
#55602=CARTESIAN_POINT('Ctrl Pts',(115.408753818094,-0.0769602871616455,
339.919377091036));
#55603=CARTESIAN_POINT('Ctrl Pts',(115.401342013917,0.0534033261641989,
339.919679690646));
#55604=CARTESIAN_POINT('Ctrl Pts',(115.39393020974,0.183378682197175,339.914830141665));
#55605=CARTESIAN_POINT('Ctrl Pts',(115.386155130962,0.319724517605634,339.909742901842));
#55606=CARTESIAN_POINT('Ctrl Pts',(115.378380052183,0.456073952128501,339.898969622455));
#55607=CARTESIAN_POINT('Ctrl Pts',(115.370604973405,0.591914113628146,339.882501484341));
#55608=CARTESIAN_POINT('Ctrl Pts',(115.362839462356,0.727587115161151,339.866053611318));
#55609=CARTESIAN_POINT('Ctrl Pts',(115.355073951307,0.862751706286306,339.843924869844));
#55610=CARTESIAN_POINT('Ctrl Pts',(115.347308440258,0.99689570957855,339.816158428325));
#55611=CARTESIAN_POINT('Ctrl Pts',(115.339550628736,1.13090670870052,339.788419517313));
#55612=CARTESIAN_POINT('Ctrl Pts',(115.331792817214,1.26389875346427,339.755054108984));
#55613=CARTESIAN_POINT('Ctrl Pts',(115.324035005691,1.39536583695736,339.716157041867));
#55614=CARTESIAN_POINT('Ctrl Pts',(115.316283032168,1.52673398730124,339.677289246027));
#55615=CARTESIAN_POINT('Ctrl Pts',(115.308531058645,1.65657908727584,339.632898187596));
#55616=CARTESIAN_POINT('Ctrl Pts',(115.300779085122,1.78440671112553,339.583129471419));
#55617=CARTESIAN_POINT('Ctrl Pts',(115.293030394565,1.91218019990054,339.533381832323));
#55618=CARTESIAN_POINT('Ctrl Pts',(115.285281704007,2.03793754841391,339.478261206671));
#55619=CARTESIAN_POINT('Ctrl Pts',(115.27753301345,2.16120106624084,339.417962541011));
#55620=CARTESIAN_POINT('Ctrl Pts',(115.269785935072,2.28443893806337,339.357676420993));
#55621=CARTESIAN_POINT('Ctrl Pts',(115.262038856694,2.40518366035942,339.292214575514));
#55622=CARTESIAN_POINT('Ctrl Pts',(115.254291778316,2.52297941726174,339.221819266924));
#55623=CARTESIAN_POINT('Ctrl Pts',(115.24654463501,2.64077616140572,339.151423368354));
#55624=CARTESIAN_POINT('Ctrl Pts',(115.238797491705,2.75562355533375,339.076094124715));
#55625=CARTESIAN_POINT('Ctrl Pts',(115.231050348399,2.86709254572145,338.996118541381));
#55626=CARTESIAN_POINT('Ctrl Pts',(115.223301463371,2.97858659670474,338.916124977838));
#55627=CARTESIAN_POINT('Ctrl Pts',(115.215552578343,3.08670041522773,338.831483223786));
#55628=CARTESIAN_POINT('Ctrl Pts',(115.207803693315,3.19103628981436,338.742521938424));
#55629=CARTESIAN_POINT('Ctrl Pts',(115.20004658354,3.29548290757648,338.653466228635));
#55630=CARTESIAN_POINT('Ctrl Pts',(115.192289473765,3.3961432732495,338.560082082984));
#55631=CARTESIAN_POINT('Ctrl Pts',(115.18453236399,3.49265457077679,338.462736939436));
#55632=CARTESIAN_POINT('Ctrl Pts',(115.176771109064,3.58921744085566,338.365339777755));
#55633=CARTESIAN_POINT('Ctrl Pts',(115.169009854138,3.68162656175378,338.263977689305));
#55634=CARTESIAN_POINT('Ctrl Pts',(115.161248599212,3.76955869310252,338.159052123938));
#55635=CARTESIAN_POINT('Ctrl Pts',(115.153474928807,3.85763148720447,338.053958711861));
#55636=CARTESIAN_POINT('Ctrl Pts',(115.145701258403,3.94121274208253,337.945290741769));
#55637=CARTESIAN_POINT('Ctrl Pts',(115.137927587998,4.02002141170511,337.833480353193));
#55638=CARTESIAN_POINT('Ctrl Pts',(115.130515783821,4.09516151879633,337.726874765107));
#55639=CARTESIAN_POINT('Ctrl Pts',(115.123103979644,4.16596321269736,337.617412975488));
#55640=CARTESIAN_POINT('Ctrl Pts',(115.115692175467,4.23222224663177,337.505489556477));
#55641=CARTESIAN_POINT('Ctrl Pts',(115.107917096688,4.30172883319483,337.388080437297));
#55642=CARTESIAN_POINT('Ctrl Pts',(115.10014201791,4.3664558554701,337.267591249273));
#55643=CARTESIAN_POINT('Ctrl Pts',(115.092366939131,4.42611835269136,337.14444850497));
#55644=CARTESIAN_POINT('Ctrl Pts',(115.084601428082,4.48570743141148,337.021457295654));
#55645=CARTESIAN_POINT('Ctrl Pts',(115.076835917033,4.54024421661018,336.895819375608));
#55646=CARTESIAN_POINT('Ctrl Pts',(115.069070405984,4.58948784092821,336.767988806659));
#55647=CARTESIAN_POINT('Ctrl Pts',(115.061312594462,4.63868264004919,336.640284982092));
#55648=CARTESIAN_POINT('Ctrl Pts',(115.05355478294,4.68259458286879,336.510393197436));
#55649=CARTESIAN_POINT('Ctrl Pts',(115.045796971418,4.72102959175553,336.378790287269));
#55650=CARTESIAN_POINT('Ctrl Pts',(115.038044997895,4.75943567707948,336.247286412466));
#55651=CARTESIAN_POINT('Ctrl Pts',(115.030293024372,4.79237292310994,336.114074348898));
#55652=CARTESIAN_POINT('Ctrl Pts',(115.022541050849,4.81969620992057,335.979648664868));
#55653=CARTESIAN_POINT('Ctrl Pts',(115.014792360291,4.84700792530293,335.845279910195));
#55654=CARTESIAN_POINT('Ctrl Pts',(115.007043669733,4.86871033248061,335.709698939554));
#55655=CARTESIAN_POINT('Ctrl Pts',(114.999294979176,4.88470886046739,335.573412949776));
#55656=CARTESIAN_POINT('Ctrl Pts',(114.991547900798,4.90070405982682,335.437155315437));
#55657=CARTESIAN_POINT('Ctrl Pts',(114.98380082242,4.91099769496158,335.300193341694));
#55658=CARTESIAN_POINT('Ctrl Pts',(114.976053744042,4.91554682132943,335.163041435893));
#55659=CARTESIAN_POINT('Ctrl Pts',(114.968306600736,4.92009598582334,335.025888380627));
#55660=CARTESIAN_POINT('Ctrl Pts',(114.960559457431,4.9189005325649,334.888545780787));
#55661=CARTESIAN_POINT('Ctrl Pts',(114.952812314125,4.91196962512306,334.751529751543));
#55662=CARTESIAN_POINT('Ctrl Pts',(114.945063429097,4.9050371594661,334.614482918187));
#55663=CARTESIAN_POINT('Ctrl Pts',(114.937314544069,4.89236669350375,334.477763191824));
#55664=CARTESIAN_POINT('Ctrl Pts',(114.929565659041,4.87401937926774,334.34188287287));
#55665=CARTESIAN_POINT('Ctrl Pts',(114.921808549266,4.85565259100276,334.20585832914));
#55666=CARTESIAN_POINT('Ctrl Pts',(114.914051439491,4.83159697041761,334.070675360558));
#55667=CARTESIAN_POINT('Ctrl Pts',(114.906294329716,4.80196516334924,333.936837908652));
#55668=CARTESIAN_POINT('Ctrl Pts',(114.89853307479,4.77231752199068,333.802928938291));
#55669=CARTESIAN_POINT('Ctrl Pts',(114.890771819864,4.73708785710019,333.67036729485));
#55670=CARTESIAN_POINT('Ctrl Pts',(114.883010564938,4.69643883251175,333.539642045601));
#55671=CARTESIAN_POINT('Ctrl Pts',(114.875236894533,4.65572478273139,333.408707678557));
#55672=CARTESIAN_POINT('Ctrl Pts',(114.867463224128,4.60957418125725,333.279615944218));
#55673=CARTESIAN_POINT('Ctrl Pts',(114.859689553724,4.55819833330779,333.152837035687));
#55674=CARTESIAN_POINT('Ctrl Pts',(114.852277749547,4.50921404344014,333.031959715847));
#55675=CARTESIAN_POINT('Ctrl Pts',(114.844865945369,4.4554801484547,332.913185005678));
#55676=CARTESIAN_POINT('Ctrl Pts',(114.837454141192,4.39721792283059,332.796898186275));
#55677=CARTESIAN_POINT('Ctrl Pts',(114.829679062414,4.33610009197499,332.674911803454));
#55678=CARTESIAN_POINT('Ctrl Pts',(114.821903983635,4.26980566903004,332.555277856224));
#55679=CARTESIAN_POINT('Ctrl Pts',(114.814128904857,4.19853910889006,332.438466784596));
#55680=CARTESIAN_POINT('Ctrl Pts',(114.806363393808,4.12736024678934,332.321799456427));
#55681=CARTESIAN_POINT('Ctrl Pts',(114.798597882759,4.05122162324646,332.207948422623));
#55682=CARTESIAN_POINT('Ctrl Pts',(114.79083237171,3.97037472138839,332.097361952592));
#55683=CARTESIAN_POINT('Ctrl Pts',(114.783074560188,3.88960797946899,331.986885129368));
#55684=CARTESIAN_POINT('Ctrl Pts',(114.775316748666,3.80414247855796,331.879666741964));
#55685=CARTESIAN_POINT('Ctrl Pts',(114.767558937143,3.71427417248259,331.776128036952));
#55686=CARTESIAN_POINT('Ctrl Pts',(114.75980696362,3.62447349515731,331.672667248098));
#55687=CARTESIAN_POINT('Ctrl Pts',(114.752054990097,3.53027686271404,331.572880923922));
#55688=CARTESIAN_POINT('Ctrl Pts',(114.744303016574,3.43202163547017,331.477158738154));
#55689=CARTESIAN_POINT('Ctrl Pts',(114.736554326017,3.33380801937357,331.381477090788));
#55690=CARTESIAN_POINT('Ctrl Pts',(114.728805635459,3.23153950647545,331.289856430743));
#55691=CARTESIAN_POINT('Ctrl Pts',(114.721056944901,3.12559143162631,331.202650758089));
#55692=CARTESIAN_POINT('Ctrl Pts',(114.713309866524,3.01966540015896,331.115463229303));
#55693=CARTESIAN_POINT('Ctrl Pts',(114.705562788146,2.91006163110279,331.032689109044));
#55694=CARTESIAN_POINT('Ctrl Pts',(114.697815709768,2.79718946081311,330.954642885626));
#55695=CARTESIAN_POINT('Ctrl Pts',(114.690068566462,2.68431634454577,330.876596008106));
#55696=CARTESIAN_POINT('Ctrl Pts',(114.682321423156,2.56817509391059,330.803277328764));
#55697=CARTESIAN_POINT('Ctrl Pts',(114.674574279851,2.44920468009787,330.734958441294));
#55698=CARTESIAN_POINT('Ctrl Pts',(114.666825394822,2.33020751921072,330.666624194288));
#55699=CARTESIAN_POINT('Ctrl Pts',(114.659076509794,2.20838026836055,330.603292170517));
#55700=CARTESIAN_POINT('Ctrl Pts',(114.651327624766,2.08418682477,330.545188181084));
#55701=CARTESIAN_POINT('Ctrl Pts',(114.643570514992,1.95986156097518,330.487022519476));
#55702=CARTESIAN_POINT('Ctrl Pts',(114.635813405217,1.83316544208234,330.434096142933));
#55703=CARTESIAN_POINT('Ctrl Pts',(114.628056295442,1.70458320240005,330.386587036846));
#55704=CARTESIAN_POINT('Ctrl Pts',(114.620295040516,1.57593225247996,330.339052543412));
#55705=CARTESIAN_POINT('Ctrl Pts',(114.61253378559,1.44539354528147,330.296941208559));
#55706=CARTESIAN_POINT('Ctrl Pts',(114.604772530664,1.31346637464161,330.260380907163));
#55707=CARTESIAN_POINT('Ctrl Pts',(114.596998860259,1.18132816352396,330.2237621212));
#55708=CARTESIAN_POINT('Ctrl Pts',(114.589225189854,1.04779743148864,330.192712201827));
#55709=CARTESIAN_POINT('Ctrl Pts',(114.58145151945,0.913383923324057,330.167307906445));
#55710=CARTESIAN_POINT('Ctrl Pts',(114.574039715273,0.785227396304288,330.143086187125));
#55711=CARTESIAN_POINT('Ctrl Pts',(114.566627911096,0.656268714751831,330.123996354817));
#55712=CARTESIAN_POINT('Ctrl Pts',(114.559216106919,0.52695161407784,330.1100608328));
#55713=CARTESIAN_POINT('Ctrl Pts',(114.55144102814,0.391296297082119,330.095442289336));
#55714=CARTESIAN_POINT('Ctrl Pts',(114.543665949362,0.254817842349541,330.086449890479));
#55715=CARTESIAN_POINT('Ctrl Pts',(114.535890870584,0.118022495196177,330.08316628783));
#55716=CARTESIAN_POINT('Ctrl Pts',(114.528125359535,-0.0186045165733258,
330.079886725863));
#55717=CARTESIAN_POINT('Ctrl Pts',(114.520359848486,-0.155547257836182,
330.082301991585));
#55718=CARTESIAN_POINT('Ctrl Pts',(114.512594337437,-0.292292677332945,
330.090443191766));
#55719=CARTESIAN_POINT('Ctrl Pts',(114.504836525914,-0.428902513348433,
330.098576319924));
#55720=CARTESIAN_POINT('Ctrl Pts',(114.497078714392,-0.56531502927271,330.112424061352));
#55721=CARTESIAN_POINT('Ctrl Pts',(114.48932090287,-0.701015832278744,330.131965502855));
#55722=CARTESIAN_POINT('Ctrl Pts',(114.481568929347,-0.836614516127381,
330.151492238803));
#55723=CARTESIAN_POINT('Ctrl Pts',(114.473816955824,-0.971502167790937,
330.176704090872));
#55724=CARTESIAN_POINT('Ctrl Pts',(114.466064982301,-1.10516853729211,330.207528240388));
#55725=CARTESIAN_POINT('Ctrl Pts',(114.458316291743,-1.23877829900636,330.238339335858));
#55726=CARTESIAN_POINT('Ctrl Pts',(114.450567601186,-1.37116742717439,330.274757913814));
#55727=CARTESIAN_POINT('Ctrl Pts',(114.442818910628,-1.50183512036135,330.316659916924));
#55728=CARTESIAN_POINT('Ctrl Pts',(114.43507183225,-1.63247562704337,330.358553201972));
#55729=CARTESIAN_POINT('Ctrl Pts',(114.427324753873,-1.76139503917644,330.405927523615));
#55730=CARTESIAN_POINT('Ctrl Pts',(114.419577675495,-1.88810738143914,330.458608849851));
#55731=CARTESIAN_POINT('Ctrl Pts',(114.411830532189,-2.01482078567322,330.511290617607));
#55732=CARTESIAN_POINT('Ctrl Pts',(114.404083388883,-2.13932672221883,330.569279328614));
#55733=CARTESIAN_POINT('Ctrl Pts',(114.396336245577,-2.26115924964645,330.632352817564));
#55734=CARTESIAN_POINT('Ctrl Pts',(114.388587360549,-2.38301916761315,330.695440486774));
#55735=CARTESIAN_POINT('Ctrl Pts',(114.380838475521,-2.50220413341341,330.763615029031));
#55736=CARTESIAN_POINT('Ctrl Pts',(114.373089590493,-2.61827321626783,330.836608542609));
#55737=CARTESIAN_POINT('Ctrl Pts',(114.365332480718,-2.73446549604562,330.909679532256));
#55738=CARTESIAN_POINT('Ctrl Pts',(114.357575370943,-2.84753495496961,330.987579502314));
#55739=CARTESIAN_POINT('Ctrl Pts',(114.349818261169,-2.9570696037799,331.069997147469));
#55740=CARTESIAN_POINT('Ctrl Pts',(114.342057006243,-3.06666278440428,331.152458833978));
#55741=CARTESIAN_POINT('Ctrl Pts',(114.334295751316,-3.17271708906238,331.239442758146));
#55742=CARTESIAN_POINT('Ctrl Pts',(114.32653449639,-3.2748547884988,331.330598253564));
#55743=CARTESIAN_POINT('Ctrl Pts',(114.318760825986,-3.37715587496764,331.421899568068));
#55744=CARTESIAN_POINT('Ctrl Pts',(114.310987155581,-3.47552755568549,331.517385516373));
#55745=CARTESIAN_POINT('Ctrl Pts',(114.303213485176,-3.56962943156249,331.616668981045));
#55746=CARTESIAN_POINT('Ctrl Pts',(114.295801680999,-3.6593508424778,331.711330776551));
#55747=CARTESIAN_POINT('Ctrl Pts',(114.288389876822,-3.74519083196599,331.809444279446));
#55748=CARTESIAN_POINT('Ctrl Pts',(114.280978072645,-3.82689041312112,331.91064847768));
#55749=CARTESIAN_POINT('Ctrl Pts',(114.273096376973,-3.91376956154956,332.018268791464));
#55750=CARTESIAN_POINT('Ctrl Pts',(114.2652146813,-3.99625251524312,332.12973910162));
#55751=CARTESIAN_POINT('Ctrl Pts',(114.257332985628,-4.07397831343783,332.244662676887));
#55752=CARTESIAN_POINT('Ctrl Pts',(114.24959039858,-4.15033228387286,332.357557899221));
#55753=CARTESIAN_POINT('Ctrl Pts',(114.241847811533,-4.22209536857364,332.473785176595));
#55754=CARTESIAN_POINT('Ctrl Pts',(114.234105224486,-4.28896385994519,332.592932890303));
#55755=CARTESIAN_POINT('Ctrl Pts',(114.226370083379,-4.35576804479946,332.711966021278));
#55756=CARTESIAN_POINT('Ctrl Pts',(114.218634942272,-4.41768680853792,332.833913661757));
#55757=CARTESIAN_POINT('Ctrl Pts',(114.210899801165,-4.47445926984854,332.958334673614));
#55758=CARTESIAN_POINT('Ctrl Pts',(114.20317040219,-4.5311895864961,333.082663322352));
#55759=CARTESIAN_POINT('Ctrl Pts',(114.195441003214,-4.58278103946054,333.209461333341));
#55760=CARTESIAN_POINT('Ctrl Pts',(114.187711604238,-4.62901851245242,333.338262754262));
#55761=CARTESIAN_POINT('Ctrl Pts',(114.179720418594,-4.67682200035038,333.471426544751));
#55762=CARTESIAN_POINT('Ctrl Pts',(114.17172923295,-4.71890222308606,333.606731473012));
#55763=CARTESIAN_POINT('Ctrl Pts',(114.163738047306,-4.75507534014221,333.743639553284));
#55764=CARTESIAN_POINT('Ctrl Pts',(114.15601424407,-4.79003811675802,333.875966734822));
#55765=CARTESIAN_POINT('Ctrl Pts',(114.148290440834,-4.81948264477097,334.00979109895));
#55766=CARTESIAN_POINT('Ctrl Pts',(114.140566637598,-4.84329371029037,334.144611726547));
#55767=CARTESIAN_POINT('Ctrl Pts',(114.132441760749,-4.86834121202774,334.286433179316));
#55768=CARTESIAN_POINT('Ctrl Pts',(114.124316883901,-4.88715441838337,334.429356673909));
#55769=CARTESIAN_POINT('Ctrl Pts',(114.116192007053,-4.89966052700142,334.572788363169));
#55770=CARTESIAN_POINT('Ctrl Pts',(114.108067130205,-4.91216663561948,334.716220052429));
#55771=CARTESIAN_POINT('Ctrl Pts',(114.099942253356,-4.91836562276903,334.860159431135));
#55772=CARTESIAN_POINT('Ctrl Pts',(114.091817376508,-4.91824836605085,335.004009032065));
#55773=CARTESIAN_POINT('',(112.341817415646,-4.92215159501353,335.000927415304));
#55774=CARTESIAN_POINT('Ctrl Pts',(114.09181737646,-4.91824836605016,335.004009032921));
#55775=CARTESIAN_POINT('Ctrl Pts',(114.082676714162,-4.91811644967628,335.165842947251));
#55776=CARTESIAN_POINT('Ctrl Pts',(114.073536051864,-4.90999303901002,335.32733713016));
#55777=CARTESIAN_POINT('Ctrl Pts',(114.064395389566,-4.89400164464294,335.487781677323));
#55778=CARTESIAN_POINT('Ctrl Pts',(114.055191910065,-4.87790035291416,335.64932884456));
#55779=CARTESIAN_POINT('Ctrl Pts',(114.045988430563,-4.8538226684699,335.809811838755));
#55780=CARTESIAN_POINT('Ctrl Pts',(114.036784951062,-4.82194352195957,335.96852657864));
#55781=CARTESIAN_POINT('Ctrl Pts',(114.027512341879,-4.78982492305096,336.128433465407));
#55782=CARTESIAN_POINT('Ctrl Pts',(114.018239732696,-4.74978729078376,336.28654537743));
#55783=CARTESIAN_POINT('Ctrl Pts',(114.008967123514,-4.70205766064995,336.442163936043));
#55784=CARTESIAN_POINT('Ctrl Pts',(114.006891428466,-4.69137327236871,336.476999510912));
#55785=CARTESIAN_POINT('Ctrl Pts',(114.004815733418,-4.68030362671436,336.511710231549));
#55786=CARTESIAN_POINT('Ctrl Pts',(114.002740038371,-4.66885159300798,336.546288415842));
#55787=CARTESIAN_POINT('Ctrl Pts',(113.994964959592,-4.62595489469636,336.675810383539));
#55788=CARTESIAN_POINT('Ctrl Pts',(113.987189880814,-4.57759658448115,336.803750626139));
#55789=CARTESIAN_POINT('Ctrl Pts',(113.979414802036,-4.5239111738125,336.929614146392));
#55790=CARTESIAN_POINT('Ctrl Pts',(113.971649290987,-4.47029182645941,337.05532278357));
#55791=CARTESIAN_POINT('Ctrl Pts',(113.963883779938,-4.41135857378103,337.178959427094));
#55792=CARTESIAN_POINT('Ctrl Pts',(113.956118268889,-4.34729566000345,337.30004424023));
#55793=CARTESIAN_POINT('Ctrl Pts',(113.948360457366,-4.2832962647914,337.421008997421));
#55794=CARTESIAN_POINT('Ctrl Pts',(113.940602645844,-4.21417751167162,337.539426616088));
#55795=CARTESIAN_POINT('Ctrl Pts',(113.932844834322,-4.14017154621386,337.654837590215));
#55796=CARTESIAN_POINT('Ctrl Pts',(113.925092860799,-4.06622127259198,337.770161713926));
#55797=CARTESIAN_POINT('Ctrl Pts',(113.917340887276,-3.98739131721963,337.88248336897));
#55798=CARTESIAN_POINT('Ctrl Pts',(113.909588913753,-3.90395935062811,337.991368324219));
#55799=CARTESIAN_POINT('Ctrl Pts',(113.901840223195,-3.82056271752398,338.100207166625));
#55800=CARTESIAN_POINT('Ctrl Pts',(113.894091532638,-3.73256818677585,338.205611894393));
#55801=CARTESIAN_POINT('Ctrl Pts',(113.88634284208,-3.6402961488424,338.307178103947));
#55802=CARTESIAN_POINT('Ctrl Pts',(113.878595763702,-3.54804330887711,338.408723181801));
#55803=CARTESIAN_POINT('Ctrl Pts',(113.870848685324,-3.45151499461248,338.506431040856));
#55804=CARTESIAN_POINT('Ctrl Pts',(113.863101606946,-3.35107093811122,338.599931475771));
#55805=CARTESIAN_POINT('Ctrl Pts',(113.855354463641,-3.25062603979216,338.693432694309));
#55806=CARTESIAN_POINT('Ctrl Pts',(113.847607320335,-3.14626561988103,338.78272615205));
#55807=CARTESIAN_POINT('Ctrl Pts',(113.839860177029,-3.03838491857391,338.867479818833));
#55808=CARTESIAN_POINT('Ctrl Pts',(113.832111292001,-2.93047996339461,338.95225254004));
#55809=CARTESIAN_POINT('Ctrl Pts',(113.824362406973,-2.81905345925911,339.032483197902));
#55810=CARTESIAN_POINT('Ctrl Pts',(113.816613521945,-2.70453191113264,339.107881473967));
#55811=CARTESIAN_POINT('Ctrl Pts',(113.80885641217,-2.58988880865183,339.183359778543));
#55812=CARTESIAN_POINT('Ctrl Pts',(113.801099302395,-2.47214442684781,339.253995240104));
#55813=CARTESIAN_POINT('Ctrl Pts',(113.793342192621,-2.35175278369957,339.319541863075));
#55814=CARTESIAN_POINT('Ctrl Pts',(113.785580937694,-2.23129680710669,339.385123512066));
#55815=CARTESIAN_POINT('Ctrl Pts',(113.777819682768,-2.10819110106501,339.445610731708));
#55816=CARTESIAN_POINT('Ctrl Pts',(113.770058427842,-1.98291131389037,339.500805015077));
#55817=CARTESIAN_POINT('Ctrl Pts',(113.762284757437,-1.85743111988475,339.556087591312));
#55818=CARTESIAN_POINT('Ctrl Pts',(113.754511087033,-1.72977025920189,339.606060169199));
#55819=CARTESIAN_POINT('Ctrl Pts',(113.746737416628,-1.60042208996249,339.650573319115));
#55820=CARTESIAN_POINT('Ctrl Pts',(113.739325612451,-1.47709510912091,339.693014371192));
#55821=CARTESIAN_POINT('Ctrl Pts',(113.731913808274,-1.35223464861885,339.730492746943));
#55822=CARTESIAN_POINT('Ctrl Pts',(113.724502004097,-1.22627657812866,339.762922297963));
#55823=CARTESIAN_POINT('Ctrl Pts',(113.716726925318,-1.09414492739364,339.796941317882));
#55824=CARTESIAN_POINT('Ctrl Pts',(113.70895184654,-0.960387791449329,339.825511589623));
#55825=CARTESIAN_POINT('Ctrl Pts',(113.701176767762,-0.825494215907046,
339.84847835532));
#55826=CARTESIAN_POINT('Ctrl Pts',(113.693411256713,-0.690766635497214,
339.871416858949));
#55827=CARTESIAN_POINT('Ctrl Pts',(113.685645745664,-0.55490577967201,339.888765511566));
#55828=CARTESIAN_POINT('Ctrl Pts',(113.677880234615,-0.418414858500553,
339.900419580881));
#55829=CARTESIAN_POINT('Ctrl Pts',(113.670122423092,-0.282059268474728,
339.912062095153));
#55830=CARTESIAN_POINT('Ctrl Pts',(113.66236461157,-0.145075243262551,339.918021229332));
#55831=CARTESIAN_POINT('Ctrl Pts',(113.654606800048,-0.00797481856245829,
339.918243534512));
#55832=CARTESIAN_POINT('Ctrl Pts',(113.646854826525,0.129022433720157,339.9184656724));
#55833=CARTESIAN_POINT('Ctrl Pts',(113.639102853002,0.26613552183858,339.912959573724));
#55834=CARTESIAN_POINT('Ctrl Pts',(113.631350879479,0.402849028114068,339.901723750177));
#55835=CARTESIAN_POINT('Ctrl Pts',(113.623602188921,0.539504636138481,339.890492685008));
#55836=CARTESIAN_POINT('Ctrl Pts',(113.615853498364,0.675760610142744,339.873536753138));
#55837=CARTESIAN_POINT('Ctrl Pts',(113.608104807806,0.811103496870204,339.850906531759));
#55838=CARTESIAN_POINT('Ctrl Pts',(113.600357729428,0.946418224379767,339.828281018787));
#55839=CARTESIAN_POINT('Ctrl Pts',(113.59261065105,1.08081985720693,339.799983628991));
#55840=CARTESIAN_POINT('Ctrl Pts',(113.584863572673,1.21380241012255,339.766116529385));
#55841=CARTESIAN_POINT('Ctrl Pts',(113.577116429367,1.34678607755987,339.732249145941));
#55842=CARTESIAN_POINT('Ctrl Pts',(113.569369286061,1.47835026258007,339.692812056047));
#55843=CARTESIAN_POINT('Ctrl Pts',(113.561622142755,1.60800186678905,339.647957945045));
#55844=CARTESIAN_POINT('Ctrl Pts',(113.553873257727,1.73768261943124,339.603093749886));
#55845=CARTESIAN_POINT('Ctrl Pts',(113.546124372699,1.86544956631175,339.552810237981));
#55846=CARTESIAN_POINT('Ctrl Pts',(113.538375487671,1.99082776614344,339.497308958483));
#55847=CARTESIAN_POINT('Ctrl Pts',(113.530618377896,2.11633904369191,339.441748769353));
#55848=CARTESIAN_POINT('Ctrl Pts',(113.522861268121,2.23945615142586,339.380959908041));
#55849=CARTESIAN_POINT('Ctrl Pts',(113.515104158347,2.35972653123695,339.315191045629));
#55850=CARTESIAN_POINT('Ctrl Pts',(113.507342903421,2.48006117969343,339.24938703844));
#55851=CARTESIAN_POINT('Ctrl Pts',(113.499581648494,2.59754573447187,339.178597929188));
#55852=CARTESIAN_POINT('Ctrl Pts',(113.491820393568,2.7117558662681,339.103116277204));
#55853=CARTESIAN_POINT('Ctrl Pts',(113.484046723164,2.82614869705421,339.027513879177));
#55854=CARTESIAN_POINT('Ctrl Pts',(113.476273052759,2.93725632081177,338.947204167224));
#55855=CARTESIAN_POINT('Ctrl Pts',(113.468499382354,3.04468609459395,338.862521151772));
#55856=CARTESIAN_POINT('Ctrl Pts',(113.461087578177,3.14711498656046,338.781780151063));
#55857=CARTESIAN_POINT('Ctrl Pts',(113.453675774,3.24620051196466,338.697064025672));
#55858=CARTESIAN_POINT('Ctrl Pts',(113.446263969823,3.34163435268695,338.608692687864));
#55859=CARTESIAN_POINT('Ctrl Pts',(113.438488891045,3.44174569022572,338.515990007545));
#55860=CARTESIAN_POINT('Ctrl Pts',(113.430713812266,3.53815470249504,338.418971791747));
#55861=CARTESIAN_POINT('Ctrl Pts',(113.422938733488,3.63046659966161,338.317965540997));
#55862=CARTESIAN_POINT('Ctrl Pts',(113.415173222439,3.72266490116185,338.217083584868));
#55863=CARTESIAN_POINT('Ctrl Pts',(113.40740771139,3.81077585804598,338.112223644137));
#55864=CARTESIAN_POINT('Ctrl Pts',(113.399642200341,3.89443908285492,338.003752202235));
#55865=CARTESIAN_POINT('Ctrl Pts',(113.391884388819,3.97801935533294,337.895388310083));
#55866=CARTESIAN_POINT('Ctrl Pts',(113.384126577296,4.05716043458111,337.783420350296));
#55867=CARTESIAN_POINT('Ctrl Pts',(113.376368765774,4.13154028237513,337.668249980345));
#55868=CARTESIAN_POINT('Ctrl Pts',(113.368616792251,4.20586415697486,337.55316627975));
#55869=CARTESIAN_POINT('Ctrl Pts',(113.360864818728,4.27543372065897,337.434885292838));
#55870=CARTESIAN_POINT('Ctrl Pts',(113.353112845205,4.3399687997975,337.313839639924));
#55871=CARTESIAN_POINT('Ctrl Pts',(113.345364154648,4.40447654829175,337.192845249916));
#55872=CARTESIAN_POINT('Ctrl Pts',(113.33761546409,4.46395386934341,337.069088866816));
#55873=CARTESIAN_POINT('Ctrl Pts',(113.329866773532,4.51816543537293,336.943029634643));
#55874=CARTESIAN_POINT('Ctrl Pts',(113.322119695154,4.57236572223335,336.816996630146));
#55875=CARTESIAN_POINT('Ctrl Pts',(113.314372616777,4.62130227894242,336.688662088447));
#55876=CARTESIAN_POINT('Ctrl Pts',(113.306625538399,4.66478720228103,336.558506791751));
#55877=CARTESIAN_POINT('Ctrl Pts',(113.298878395093,4.70827249006515,336.428350404229));
#55878=CARTESIAN_POINT('Ctrl Pts',(113.291131251787,4.74630592948563,336.296373602006));
#55879=CARTESIAN_POINT('Ctrl Pts',(113.283384108481,4.77874907306849,336.163073668839));
#55880=CARTESIAN_POINT('Ctrl Pts',(113.275635223453,4.81119951055879,336.029743767018));
#55881=CARTESIAN_POINT('Ctrl Pts',(113.267886338425,4.83805705886931,335.895090522039));
#55882=CARTESIAN_POINT('Ctrl Pts',(113.260137453397,4.8592341870001,335.759622391975));
#55883=CARTESIAN_POINT('Ctrl Pts',(113.252380343622,4.8804337927535,335.624010474638));
#55884=CARTESIAN_POINT('Ctrl Pts',(113.244623233848,4.89594087385555,335.487582331236));
#55885=CARTESIAN_POINT('Ctrl Pts',(113.236866124073,4.90571963796484,335.350853097729));
#55886=CARTESIAN_POINT('Ctrl Pts',(113.229104869147,4.91550362753301,335.214050800492));
#55887=CARTESIAN_POINT('Ctrl Pts',(113.221343614221,4.91955318919733,335.076947483062));
#55888=CARTESIAN_POINT('Ctrl Pts',(113.213582359295,4.91788471340464,334.940058293643));
#55889=CARTESIAN_POINT('Ctrl Pts',(113.20580868889,4.91621356859443,334.802950126134));
#55890=CARTESIAN_POINT('Ctrl Pts',(113.198035018485,4.90880612905042,334.666057161631));
#55891=CARTESIAN_POINT('Ctrl Pts',(113.190261348081,4.89573078963655,334.529890334172));
#55892=CARTESIAN_POINT('Ctrl Pts',(113.182849543903,4.88326411041796,334.40006210529));
#55893=CARTESIAN_POINT('Ctrl Pts',(113.175437739726,4.86564537656034,334.27089421662));
#55894=CARTESIAN_POINT('Ctrl Pts',(113.168025935549,4.84297676048445,334.142819062328));
#55895=CARTESIAN_POINT('Ctrl Pts',(113.160250856771,4.81919708800866,334.008466563211));
#55896=CARTESIAN_POINT('Ctrl Pts',(113.152475777992,4.78978484903819,333.874892044525));
#55897=CARTESIAN_POINT('Ctrl Pts',(113.144700699214,4.7548018023207,333.742604722791));
#55898=CARTESIAN_POINT('Ctrl Pts',(113.136935188165,4.71986180446933,333.610480189028));
#55899=CARTESIAN_POINT('Ctrl Pts',(113.129169677116,4.67936473779544,333.479640074828));
#55900=CARTESIAN_POINT('Ctrl Pts',(113.121404166067,4.63342375970188,333.350585762905));
#55901=CARTESIAN_POINT('Ctrl Pts',(113.113646354544,4.58752833222185,333.221659408709));
#55902=CARTESIAN_POINT('Ctrl Pts',(113.105888543022,4.53619986520041,333.094515699008));
#55903=CARTESIAN_POINT('Ctrl Pts',(113.0981307315,4.47960184761256,332.969642802518));
#55904=CARTESIAN_POINT('Ctrl Pts',(113.090378757977,4.42304642182784,332.844863876843));
#55905=CARTESIAN_POINT('Ctrl Pts',(113.082626784454,4.36122949932981,332.72235271756));
#55906=CARTESIAN_POINT('Ctrl Pts',(113.074874810931,4.29436326174215,332.602579044327));
#55907=CARTESIAN_POINT('Ctrl Pts',(113.067126120373,4.22752534204577,332.482856095316));
#55908=CARTESIAN_POINT('Ctrl Pts',(113.059377429816,4.15564255049942,332.365868667115));
#55909=CARTESIAN_POINT('Ctrl Pts',(113.051628739258,4.07897364184698,332.252063120882));
#55910=CARTESIAN_POINT('Ctrl Pts',(113.04388166088,4.00232068480135,332.138281252843));
#55911=CARTESIAN_POINT('Ctrl Pts',(113.036134582502,3.92088380960276,332.027680273942));
#55912=CARTESIAN_POINT('Ctrl Pts',(113.028387504125,3.83496563105287,331.920678374846));
#55913=CARTESIAN_POINT('Ctrl Pts',(113.020640360819,3.74904673242589,331.81367557897));
#55914=CARTESIAN_POINT('Ctrl Pts',(113.012893217513,3.6586467002629,331.710272227843));
#55915=CARTESIAN_POINT('Ctrl Pts',(113.005146074207,3.56410878921342,331.610853853675));
#55916=CARTESIAN_POINT('Ctrl Pts',(112.997397189179,3.4695496240345,331.511413128146));
#55917=CARTESIAN_POINT('Ctrl Pts',(112.989648304151,3.37085099810707,331.415959445531));
#55918=CARTESIAN_POINT('Ctrl Pts',(112.981899419123,3.26839311662505,331.324841568354));
#55919=CARTESIAN_POINT('Ctrl Pts',(112.974142309348,3.16582648528896,331.233626977721));
#55920=CARTESIAN_POINT('Ctrl Pts',(112.966385199573,3.05949292031569,331.146757645753));
#55921=CARTESIAN_POINT('Ctrl Pts',(112.958628089799,2.94980624123419,331.064542440621));
#55922=CARTESIAN_POINT('Ctrl Pts',(112.950866834872,2.84006094909857,330.982283302311));
#55923=CARTESIAN_POINT('Ctrl Pts',(112.943105579946,2.72695929468062,330.904683467466));
#55924=CARTESIAN_POINT('Ctrl Pts',(112.93534432502,2.61094334690706,330.832007929261));
#55925=CARTESIAN_POINT('Ctrl Pts',(112.927570654616,2.49474181142657,330.75921613388));
#55926=CARTESIAN_POINT('Ctrl Pts',(112.919796984211,2.37561700651664,330.691364569814));
#55927=CARTESIAN_POINT('Ctrl Pts',(112.912023313806,2.25403559989488,330.628672218089));
#55928=CARTESIAN_POINT('Ctrl Pts',(112.904611509629,2.13811383700298,330.56889821042));
#55929=CARTESIAN_POINT('Ctrl Pts',(112.897199705452,2.01995929589355,330.51381402339));
#55930=CARTESIAN_POINT('Ctrl Pts',(112.889787901275,1.89999087740523,330.463567731325));
#55931=CARTESIAN_POINT('Ctrl Pts',(112.882012822497,1.77414244935842,330.410858718809));
#55932=CARTESIAN_POINT('Ctrl Pts',(112.874237743718,1.64590013672735,330.363307261477));
#55933=CARTESIAN_POINT('Ctrl Pts',(112.86646266494,1.51572557174947,330.321136991357));
#55934=CARTESIAN_POINT('Ctrl Pts',(112.858697153891,1.38571119486112,330.27901861444));
#55935=CARTESIAN_POINT('Ctrl Pts',(112.850931642842,1.25376966498008,330.242268368375));
#55936=CARTESIAN_POINT('Ctrl Pts',(112.843166131793,1.12038384149275,330.211062423645));
#55937=CARTESIAN_POINT('Ctrl Pts',(112.835408320271,0.987130270437835,330.179887419701));
#55938=CARTESIAN_POINT('Ctrl Pts',(112.827650508748,0.852435633725583,330.15424586584));
#55939=CARTESIAN_POINT('Ctrl Pts',(112.819892697226,0.716798916111024,330.1342644568));
#55940=CARTESIAN_POINT('Ctrl Pts',(112.812140723703,0.581264269427758,330.114298084403));
#55941=CARTESIAN_POINT('Ctrl Pts',(112.80438875018,0.444789338107743,330.099983435361));
#55942=CARTESIAN_POINT('Ctrl Pts',(112.796636776657,0.307883943084047,330.091396273879));
#55943=CARTESIAN_POINT('Ctrl Pts',(112.7888880861,0.171036527576332,330.082812749064));
#55944=CARTESIAN_POINT('Ctrl Pts',(112.781139395542,0.0337594002458191,
330.079951911891));
#55945=CARTESIAN_POINT('Ctrl Pts',(112.773390704984,-0.103432057249437,
330.082837721609));
#55946=CARTESIAN_POINT('Ctrl Pts',(112.765643626607,-0.240594970916021,
330.08572293091));
#55947=CARTESIAN_POINT('Ctrl Pts',(112.757896548229,-0.377671859658696,
330.094352400678));
#55948=CARTESIAN_POINT('Ctrl Pts',(112.750149469851,-0.51414729579194,330.108697962635));
#55949=CARTESIAN_POINT('Ctrl Pts',(112.742402326545,-0.650623875720788,
330.123043644822));
#55950=CARTESIAN_POINT('Ctrl Pts',(112.734655183239,-0.786498604253429,
330.14310547389));
#55951=CARTESIAN_POINT('Ctrl Pts',(112.726908039934,-0.921261524342264,
330.168803433282));
#55952=CARTESIAN_POINT('Ctrl Pts',(112.719159154905,-1.05605474199663,330.194507170121));
#55953=CARTESIAN_POINT('Ctrl Pts',(112.711410269877,-1.18973526993767,330.225849485512));
#55954=CARTESIAN_POINT('Ctrl Pts',(112.703661384849,-1.3218040754722,330.26269939221));
#55955=CARTESIAN_POINT('Ctrl Pts',(112.695904275075,-1.45401306020146,330.29958841178));
#55956=CARTESIAN_POINT('Ctrl Pts',(112.6881471653,-1.58460652815471,330.341996595004));
#55957=CARTESIAN_POINT('Ctrl Pts',(112.680390055525,-1.71310080400642,330.389743098502));
#55958=CARTESIAN_POINT('Ctrl Pts',(112.672628800599,-1.84166374309061,330.437515116204));
#55959=CARTESIAN_POINT('Ctrl Pts',(112.664867545673,-1.96812489470892,330.49063098701));
#55960=CARTESIAN_POINT('Ctrl Pts',(112.657106290747,-2.09202219158389,330.54886236874));
#55961=CARTESIAN_POINT('Ctrl Pts',(112.649332620342,-2.21611768375592,330.607186901703));
#55962=CARTESIAN_POINT('Ctrl Pts',(112.641558949937,-2.33764077884499,330.67064311693));
#55963=CARTESIAN_POINT('Ctrl Pts',(112.633785279533,-2.45615479035629,330.738957086779));
#55964=CARTESIAN_POINT('Ctrl Pts',(112.626373475356,-2.56915194611876,330.804091024896));
#55965=CARTESIAN_POINT('Ctrl Pts',(112.618961671179,-2.67941361606295,330.8736404849));
#55966=CARTESIAN_POINT('Ctrl Pts',(112.611549867002,-2.78658859004902,330.947333335653));
#55967=CARTESIAN_POINT('Ctrl Pts',(112.603813727223,-2.89845346933367,331.024250936349));
#55968=CARTESIAN_POINT('Ctrl Pts',(112.596077587444,-3.00731676404034,331.105931343334));
#55969=CARTESIAN_POINT('Ctrl Pts',(112.588341447665,-3.11274309098139,331.19211167285));
#55970=CARTESIAN_POINT('Ctrl Pts',(112.580614850363,-3.21803937524821,331.278185699501));
#55971=CARTESIAN_POINT('Ctrl Pts',(112.572888253061,-3.31990682244749,331.368748359051));
#55972=CARTESIAN_POINT('Ctrl Pts',(112.56516165576,-3.41793826010091,331.463493091674));
#55973=CARTESIAN_POINT('Ctrl Pts',(112.557442693122,-3.51587283271895,331.55814420686));
#55974=CARTESIAN_POINT('Ctrl Pts',(112.549723730485,-3.6099786550814,331.656968900253));
#55975=CARTESIAN_POINT('Ctrl Pts',(112.542004767847,-3.69988128146181,331.759620151033));
#55976=CARTESIAN_POINT('Ctrl Pts',(112.534291539137,-3.7897171248876,331.862195148715));
#55977=CARTESIAN_POINT('Ctrl Pts',(112.526578310427,-3.8753557266531,331.968590750737));
#55978=CARTESIAN_POINT('Ctrl Pts',(112.518865081717,-3.95645950875015,332.07842316238));
#55979=CARTESIAN_POINT('Ctrl Pts',(112.511154984209,-4.03753036659233,332.188210987318));
#55980=CARTESIAN_POINT('Ctrl Pts',(112.5034448867,-4.11406983101611,332.301432530293));
#55981=CARTESIAN_POINT('Ctrl Pts',(112.495734789192,-4.18578082841537,332.417671221752));
#55982=CARTESIAN_POINT('Ctrl Pts',(112.4880261404,-4.2574783514216,332.533888072128));
#55983=CARTESIAN_POINT('Ctrl Pts',(112.480317491608,-4.32434900432464,332.653120607296));
#55984=CARTESIAN_POINT('Ctrl Pts',(112.472608842816,-4.38613951426719,332.774923995931));
#55985=CARTESIAN_POINT('Ctrl Pts',(112.464899930553,-4.44793213612624,332.896731547642));
#55986=CARTESIAN_POINT('Ctrl Pts',(112.457191018289,-4.5046440908141,333.021109775104));
#55987=CARTESIAN_POINT('Ctrl Pts',(112.449482106026,-4.55606868309945,333.147590429365));
#55988=CARTESIAN_POINT('Ctrl Pts',(112.441771218253,-4.60750645360872,333.274103495946));
#55989=CARTESIAN_POINT('Ctrl Pts',(112.43406033048,-4.65365401753412,333.402719695066));
#55990=CARTESIAN_POINT('Ctrl Pts',(112.426349442707,-4.69435348447759,333.532952480227));
#55991=CARTESIAN_POINT('Ctrl Pts',(112.418630419675,-4.73509589079766,333.66332266558));
#55992=CARTESIAN_POINT('Ctrl Pts',(112.410911396643,-4.77037860415737,333.795312465115));
#55993=CARTESIAN_POINT('Ctrl Pts',(112.403192373611,-4.80009401809788,333.928421500812));
#55994=CARTESIAN_POINT('Ctrl Pts',(112.395468925079,-4.82982646859386,334.061606851095));
#55995=CARTESIAN_POINT('Ctrl Pts',(112.387745476547,-4.85398519231118,334.195912327251));
#55996=CARTESIAN_POINT('Ctrl Pts',(112.380022028015,-4.87251422816711,334.330830246642));
#55997=CARTESIAN_POINT('Ctrl Pts',(112.372287044735,-4.89107093660431,334.465949662059));
#55998=CARTESIAN_POINT('Ctrl Pts',(112.364552061455,-4.9039811281351,334.601682954669));
#55999=CARTESIAN_POINT('Ctrl Pts',(112.356817078175,-4.91124089480556,334.737519647041));
#56000=CARTESIAN_POINT('Ctrl Pts',(112.351817203424,-4.91593359067253,334.825324161127));
#56001=CARTESIAN_POINT('Ctrl Pts',(112.346817328674,-4.91826643516687,334.913171884236));
#56002=CARTESIAN_POINT('Ctrl Pts',(112.341817453923,-4.91824991282565,335.000926007804));
#56003=CARTESIAN_POINT('',(110.591817843044,-4.91738553598639,334.995487657965));
#56004=CARTESIAN_POINT('Ctrl Pts',(112.341817376508,-4.92614104176129,335.000928854464));
#56005=CARTESIAN_POINT('Ctrl Pts',(112.338982195248,-4.92627011657859,335.050769735367));
#56006=CARTESIAN_POINT('Ctrl Pts',(112.243401002563,-4.90298212628779,336.73090936613));
#56007=CARTESIAN_POINT('Ctrl Pts',(112.055073798454,-2.99650838422388,339.984514657387));
#56008=CARTESIAN_POINT('Ctrl Pts',(111.776835764179,2.57000208903517,340.2172347205));
#56009=CARTESIAN_POINT('Ctrl Pts',(111.498597729906,5.7780595783553,335.662175486868));
#56010=CARTESIAN_POINT('Ctrl Pts',(111.220359695631,3.68367707663835,330.499447582632));
#56011=CARTESIAN_POINT('Ctrl Pts',(110.942121661358,-1.7911615073251,329.466810203769));
#56012=CARTESIAN_POINT('Ctrl Pts',(110.732607789333,-4.6760006404016,332.512771583302));
#56013=CARTESIAN_POINT('Ctrl Pts',(110.615839928733,-4.92075371318481,334.571140323605));
#56014=CARTESIAN_POINT('Ctrl Pts',(110.591818079557,-4.91694833721634,334.995483880473));
#56015=CARTESIAN_POINT('',(108.84181737648,-4.91824982733306,335.001303241486));
#56016=CARTESIAN_POINT('Ctrl Pts',(110.591817376508,-4.91824793686326,334.995495109295));
#56017=CARTESIAN_POINT('Ctrl Pts',(110.584146126918,-4.91837209122975,335.131041562429));
#56018=CARTESIAN_POINT('Ctrl Pts',(110.576474877328,-4.9128885595775,335.266724912895));
#56019=CARTESIAN_POINT('Ctrl Pts',(110.568803627738,-4.90179024276939,335.402039150321));
#56020=CARTESIAN_POINT('Ctrl Pts',(110.561136543147,-4.89069795164023,335.537279920737));
#56021=CARTESIAN_POINT('Ctrl Pts',(110.553469458557,-4.87399697080814,335.672151579091));
#56022=CARTESIAN_POINT('Ctrl Pts',(110.545802373967,-4.85173227595791,335.806149480511));
#56023=CARTESIAN_POINT('Ctrl Pts',(110.538137415738,-4.82947375591737,335.940110219439));
#56024=CARTESIAN_POINT('Ctrl Pts',(110.530472457509,-4.80165465517224,336.073197288958));
#56025=CARTESIAN_POINT('Ctrl Pts',(110.52280749928,-4.7683716047274,336.204912985128));
#56026=CARTESIAN_POINT('Ctrl Pts',(110.515142921812,-4.73509020763609,336.336622138249));
#56027=CARTESIAN_POINT('Ctrl Pts',(110.507478344344,-4.69634549859154,336.466959665636));
#56028=CARTESIAN_POINT('Ctrl Pts',(110.499813766876,-4.65228472135179,336.595440357386));
#56029=CARTESIAN_POINT('Ctrl Pts',(110.492147825117,-4.60821610131729,336.723943918631));
#56030=CARTESIAN_POINT('Ctrl Pts',(110.484481883359,-4.55882966116891,336.850589608606));
#56031=CARTESIAN_POINT('Ctrl Pts',(110.4768159416,-4.50432160298151,336.974910114262));
#56032=CARTESIAN_POINT('Ctrl Pts',(110.469142147348,-4.44975771027771,337.099357965774));
#56033=CARTESIAN_POINT('Ctrl Pts',(110.461468353096,-4.39006188184791,337.221475508781));
#56034=CARTESIAN_POINT('Ctrl Pts',(110.453794558845,-4.32547749756932,337.34081769485));
#56035=CARTESIAN_POINT('Ctrl Pts',(110.446116831348,-4.26086001021524,337.460221050401));
#56036=CARTESIAN_POINT('Ctrl Pts',(110.438439103852,-4.19134918162487,337.576845872649));
#56037=CARTESIAN_POINT('Ctrl Pts',(110.430761376355,-4.11723229695039,337.69027531592));
#56038=CARTESIAN_POINT('Ctrl Pts',(110.423071357589,-4.04299675859383,337.803886348328));
#56039=CARTESIAN_POINT('Ctrl Pts',(110.415381338822,-3.96414066467786,337.914291456165));
#56040=CARTESIAN_POINT('Ctrl Pts',(110.407691320056,-3.88099269015923,338.021105559465));
#56041=CARTESIAN_POINT('Ctrl Pts',(110.400342744307,-3.80153655258109,338.123177030673));
#56042=CARTESIAN_POINT('Ctrl Pts',(110.392994168559,-3.71816169532594,338.221969332601));
#56043=CARTESIAN_POINT('Ctrl Pts',(110.38564559281,-3.63118545644224,338.317178807876));
#56044=CARTESIAN_POINT('Ctrl Pts',(110.377870514032,-3.53916121496859,338.417914133474));
#56045=CARTESIAN_POINT('Ctrl Pts',(110.370095435253,-3.44279652465389,338.514976372805));
#56046=CARTESIAN_POINT('Ctrl Pts',(110.362320356475,-3.34241621146445,338.607968532546));
#56047=CARTESIAN_POINT('Ctrl Pts',(110.354554845426,-3.24215942264098,338.700846259513));
#56048=CARTESIAN_POINT('Ctrl Pts',(110.346789334377,-3.1378971270698,338.789663609256));
#56049=CARTESIAN_POINT('Ctrl Pts',(110.339023823328,-3.02999336514519,338.874057726683));
#56050=CARTESIAN_POINT('Ctrl Pts',(110.331266011805,-2.92219659011453,338.958368167098));
#56051=CARTESIAN_POINT('Ctrl Pts',(110.323508200283,-2.81076583978284,339.038263863628));
#56052=CARTESIAN_POINT('Ctrl Pts',(110.315750388761,-2.69610058685823,339.113420071916));
#56053=CARTESIAN_POINT('Ctrl Pts',(110.307998415238,-2.58152162317276,339.188519722774));
#56054=CARTESIAN_POINT('Ctrl Pts',(110.300246441715,-2.46371332737801,339.258886771156));
#56055=CARTESIAN_POINT('Ctrl Pts',(110.292494468192,-2.34310641714275,339.324238127167));
#56056=CARTESIAN_POINT('Ctrl Pts',(110.284745777634,-2.22255058400558,339.38956180684));
#56057=CARTESIAN_POINT('Ctrl Pts',(110.276997087077,-2.09919883668719,339.449873833094));
#56058=CARTESIAN_POINT('Ctrl Pts',(110.269248396519,-1.97350871892266,339.504935781877));
#56059=CARTESIAN_POINT('Ctrl Pts',(110.261501318141,-1.84784475203692,339.559986274561));
#56060=CARTESIAN_POINT('Ctrl Pts',(110.253754239763,-1.71984374022442,339.609788705735));
#56061=CARTESIAN_POINT('Ctrl Pts',(110.246007161386,-1.58998518530124,339.654151928442));
#56062=CARTESIAN_POINT('Ctrl Pts',(110.23826001808,-1.4601255420383,339.698515522956));
#56063=CARTESIAN_POINT('Ctrl Pts',(110.230512874774,-1.32840869449841,339.737439691714));
#56064=CARTESIAN_POINT('Ctrl Pts',(110.222765731468,-1.19533097978101,339.770782630898));
#56065=CARTESIAN_POINT('Ctrl Pts',(110.21501684644,-1.06222334636803,339.804133066282));
#56066=CARTESIAN_POINT('Ctrl Pts',(110.207267961412,-0.927754616047893,
339.831899680242));
#56067=CARTESIAN_POINT('Ctrl Pts',(110.199519076384,-0.792432643955706,
339.853991508778));
#56068=CARTESIAN_POINT('Ctrl Pts',(110.191761966609,-0.656967039724294,
339.87610678581));
#56069=CARTESIAN_POINT('Ctrl Pts',(110.184004856834,-0.520646770997407,
339.892535182283));
#56070=CARTESIAN_POINT('Ctrl Pts',(110.17624774706,-0.383986720176763,339.903237426561));
#56071=CARTESIAN_POINT('Ctrl Pts',(110.168486492134,-0.247253642594687,
339.913945389776));
#56072=CARTESIAN_POINT('Ctrl Pts',(110.160725237207,-0.110180811545775,
339.918921089554));
#56073=CARTESIAN_POINT('Ctrl Pts',(110.152963982281,0.0267165257919835,
339.918177435773));
#56074=CARTESIAN_POINT('Ctrl Pts',(110.145190311877,0.163832854254837,339.917432592389));
#56075=CARTESIAN_POINT('Ctrl Pts',(110.137416641472,0.300772737376946,339.910950131324));
#56076=CARTESIAN_POINT('Ctrl Pts',(110.129642971067,0.437024790724611,339.898794994158));
#56077=CARTESIAN_POINT('Ctrl Pts',(110.12223116689,0.566934278208219,339.887205681552));
#56078=CARTESIAN_POINT('Ctrl Pts',(110.114819362713,0.696218246345673,339.870459970809));
#56079=CARTESIAN_POINT('Ctrl Pts',(110.107407558536,0.824443620590572,339.848657110888));
#56080=CARTESIAN_POINT('Ctrl Pts',(110.099632479758,0.958953702391189,339.825785627855));
#56081=CARTESIAN_POINT('Ctrl Pts',(110.091857400979,1.09272387351054,339.797276451051));
#56082=CARTESIAN_POINT('Ctrl Pts',(110.084082322201,1.22524451182462,339.763187897695));
#56083=CARTESIAN_POINT('Ctrl Pts',(110.076316811152,1.3576020750564,339.729141292473));
#56084=CARTESIAN_POINT('Ctrl Pts',(110.068551300103,1.48871278999301,339.689529068073));
#56085=CARTESIAN_POINT('Ctrl Pts',(110.060785789054,1.61807452090086,339.644460992119));
#56086=CARTESIAN_POINT('Ctrl Pts',(110.053027977532,1.74730798927606,339.599437601292));
#56087=CARTESIAN_POINT('Ctrl Pts',(110.045270166009,1.87479555788748,339.548969251874));
#56088=CARTESIAN_POINT('Ctrl Pts',(110.037512354487,2.00004796467262,339.493216131181));
#56089=CARTESIAN_POINT('Ctrl Pts',(110.029760380964,2.12520611505045,339.43750496648));
#56090=CARTESIAN_POINT('Ctrl Pts',(110.022008407441,2.24813209594357,339.376517104756));
#56091=CARTESIAN_POINT('Ctrl Pts',(110.014256433918,2.36835476497503,339.3104615495));
#56092=CARTESIAN_POINT('Ctrl Pts',(110.00650774336,2.48852651963404,339.244433968812));
#56093=CARTESIAN_POINT('Ctrl Pts',(109.998759052803,2.60599689760791,339.173343151008));
#56094=CARTESIAN_POINT('Ctrl Pts',(109.991010362245,2.72031779985406,339.097444829439));
#56095=CARTESIAN_POINT('Ctrl Pts',(109.983263283867,2.83461491668183,339.02156229915));
#56096=CARTESIAN_POINT('Ctrl Pts',(109.97551620549,2.94576353573271,338.940874470706));
#56097=CARTESIAN_POINT('Ctrl Pts',(109.967769127112,3.05334343150593,338.855681126828));
#56098=CARTESIAN_POINT('Ctrl Pts',(109.960021983806,3.16092422890206,338.770487068948));
#56099=CARTESIAN_POINT('Ctrl Pts',(109.9522748405,3.26493593693671,338.68078766298));
#56100=CARTESIAN_POINT('Ctrl Pts',(109.944527697194,3.36499071326769,338.586923551196));
#56101=CARTESIAN_POINT('Ctrl Pts',(109.936778812166,3.46506798403668,338.493038336766));
#56102=CARTESIAN_POINT('Ctrl Pts',(109.929029927138,3.56118626788049,338.394986820737));
#56103=CARTESIAN_POINT('Ctrl Pts',(109.92128104211,3.65299424167759,338.293146843487));
#56104=CARTESIAN_POINT('Ctrl Pts',(109.913523932335,3.74489966140663,338.191198772233));
#56105=CARTESIAN_POINT('Ctrl Pts',(109.905766822561,3.83248536994826,338.085454497988));
#56106=CARTESIAN_POINT('Ctrl Pts',(109.898009712786,3.91543971053541,337.976325744213));
#56107=CARTESIAN_POINT('Ctrl Pts',(109.89024845786,3.99843837926987,337.86713867552));
#56108=CARTESIAN_POINT('Ctrl Pts',(109.882487202933,4.07680052548278,337.754563844226));
#56109=CARTESIAN_POINT('Ctrl Pts',(109.874725948007,4.15025817555468,337.63904151895));
#56110=CARTESIAN_POINT('Ctrl Pts',(109.866952277603,4.2238333339269,337.523334395602));
#56111=CARTESIAN_POINT('Ctrl Pts',(109.859178607198,4.29248812248646,337.404670694755));
#56112=CARTESIAN_POINT('Ctrl Pts',(109.851404936793,4.35600041253313,337.283515594103));
#56113=CARTESIAN_POINT('Ctrl Pts',(109.843993132616,4.41655619019804,337.168000292534));
#56114=CARTESIAN_POINT('Ctrl Pts',(109.836581328439,4.4724373382522,337.050220580623));
#56115=CARTESIAN_POINT('Ctrl Pts',(109.829169524262,4.52349295577554,336.9305943493));
#56116=CARTESIAN_POINT('Ctrl Pts',(109.821394445484,4.57705096120053,336.805104880032));
#56117=CARTESIAN_POINT('Ctrl Pts',(109.813619366705,4.62546770153305,336.677186737851));
#56118=CARTESIAN_POINT('Ctrl Pts',(109.805844287927,4.6685164311926,336.547300033667));
#56119=CARTESIAN_POINT('Ctrl Pts',(109.798078776878,4.71151218664973,336.41757316334));
#56120=CARTESIAN_POINT('Ctrl Pts',(109.790313265829,4.74915295304581,336.285882918453));
#56121=CARTESIAN_POINT('Ctrl Pts',(109.78254775478,4.7812593018591,336.152710957216));
#56122=CARTESIAN_POINT('Ctrl Pts',(109.774789943257,4.8133338171341,336.019671036366));
#56123=CARTESIAN_POINT('Ctrl Pts',(109.767032131735,4.83988474402424,335.885152700348));
#56124=CARTESIAN_POINT('Ctrl Pts',(109.759274320213,4.8607820196859,335.749654066619));
#56125=CARTESIAN_POINT('Ctrl Pts',(109.75152234669,4.88166356948478,335.614257399909));
#56126=CARTESIAN_POINT('Ctrl Pts',(109.743770373167,4.8968998771944,335.477882288605));
#56127=CARTESIAN_POINT('Ctrl Pts',(109.736018399644,4.90641173613487,335.341038030164));
#56128=CARTESIAN_POINT('Ctrl Pts',(109.728269709086,4.91591956679747,335.204251725347));
#56129=CARTESIAN_POINT('Ctrl Pts',(109.720521018529,4.91970774342025,335.066997057684));
#56130=CARTESIAN_POINT('Ctrl Pts',(109.712772327971,4.91774882553059,334.929789235209));
#56131=CARTESIAN_POINT('Ctrl Pts',(109.705025249593,4.91579031521016,334.792609959969));
#56132=CARTESIAN_POINT('Ctrl Pts',(109.697278171215,4.90808709434732,334.65547790112));
#56133=CARTESIAN_POINT('Ctrl Pts',(109.689531092838,4.8946638484961,334.518908664882));
#56134=CARTESIAN_POINT('Ctrl Pts',(109.681783949532,4.88124049014515,334.382338284063));
#56135=CARTESIAN_POINT('Ctrl Pts',(109.674036806226,4.86209704942166,334.246331124264));
#56136=CARTESIAN_POINT('Ctrl Pts',(109.66628966292,4.83731009593355,334.111397671464));
#56137=CARTESIAN_POINT('Ctrl Pts',(109.658540777892,4.81251756981203,333.976433882759));
#56138=CARTESIAN_POINT('Ctrl Pts',(109.650791892864,4.7820790767997,333.842544665763));
#56139=CARTESIAN_POINT('Ctrl Pts',(109.643043007836,4.74612222983168,333.710229926693));
#56140=CARTESIAN_POINT('Ctrl Pts',(109.635285898061,4.71012721789476,333.577774747392));
#56141=CARTESIAN_POINT('Ctrl Pts',(109.627528788286,4.66860225428536,333.446897762121));
#56142=CARTESIAN_POINT('Ctrl Pts',(109.619771678512,4.6217249106862,333.318083856893));
#56143=CARTESIAN_POINT('Ctrl Pts',(109.612010423585,4.57482251733343,333.189201117633));
#56144=CARTESIAN_POINT('Ctrl Pts',(109.604249168659,4.52256219375378,333.062384016344));
#56145=CARTESIAN_POINT('Ctrl Pts',(109.596487913733,4.46516915532161,332.938096152372));
#56146=CARTESIAN_POINT('Ctrl Pts',(109.588714243328,4.40768430673237,332.813609468323));
#56147=CARTESIAN_POINT('Ctrl Pts',(109.580940572924,4.3450505146111,332.691660454487));
#56148=CARTESIAN_POINT('Ctrl Pts',(109.573166902519,4.27753875022061,332.572687637971));
#56149=CARTESIAN_POINT('Ctrl Pts',(109.565755098342,4.21316967470548,332.459253034687));
#56150=CARTESIAN_POINT('Ctrl Pts',(109.558343294165,4.14436669791148,332.348524024804));
#56151=CARTESIAN_POINT('Ctrl Pts',(109.550931489988,4.0713995720919,332.240853648885));
#56152=CARTESIAN_POINT('Ctrl Pts',(109.54315641121,3.99485611007735,332.127906027109));
#56153=CARTESIAN_POINT('Ctrl Pts',(109.535381332431,3.91348809164955,332.017967510562));
#56154=CARTESIAN_POINT('Ctrl Pts',(109.527606253653,3.82755972884398,331.911477766855));
#56155=CARTESIAN_POINT('Ctrl Pts',(109.519840742604,3.74173710635947,331.805119065558));
#56156=CARTESIAN_POINT('Ctrl Pts',(109.512075231555,3.65136554846989,331.702200994172));
#56157=CARTESIAN_POINT('Ctrl Pts',(109.504309720506,3.55675299277143,331.603135090865));
#56158=CARTESIAN_POINT('Ctrl Pts',(109.496551908984,3.4622342456972,331.50416741169));
#56159=CARTESIAN_POINT('Ctrl Pts',(109.488794097461,3.36348313714986,331.409044580549));
#56160=CARTESIAN_POINT('Ctrl Pts',(109.481036285939,3.26084816025649,331.318145530001));
#56161=CARTESIAN_POINT('Ctrl Pts',(109.473284312416,3.15829041943749,331.22731488387));
#56162=CARTESIAN_POINT('Ctrl Pts',(109.465532338893,3.05185491926622,331.140701949735));
#56163=CARTESIAN_POINT('Ctrl Pts',(109.45778036537,2.94192707556095,331.05864894426));
#56164=CARTESIAN_POINT('Ctrl Pts',(109.450031674812,2.83204578636343,330.976630688282));
#56165=CARTESIAN_POINT('Ctrl Pts',(109.442282984255,2.71867540786182,330.8991687534));
#56166=CARTESIAN_POINT('Ctrl Pts',(109.434534293697,2.60223433987015,330.826565023521));
#56167=CARTESIAN_POINT('Ctrl Pts',(109.426787215319,2.48581749841538,330.753976399454));
#56168=CARTESIAN_POINT('Ctrl Pts',(109.419040136942,2.36633156972565,330.68624417654));
#56169=CARTESIAN_POINT('Ctrl Pts',(109.411293058564,2.24422349684125,330.62362662028));
#56170=CARTESIAN_POINT('Ctrl Pts',(109.403545915258,2.12211440057376,330.561008539224));
#56171=CARTESIAN_POINT('Ctrl Pts',(109.395798771952,1.99738346408768,330.503505388679));
#56172=CARTESIAN_POINT('Ctrl Pts',(109.388051628646,1.87050140214203,330.451329032884));
#56173=CARTESIAN_POINT('Ctrl Pts',(109.380302743618,1.74359081441508,330.399140946736));
#56174=CARTESIAN_POINT('Ctrl Pts',(109.37255385859,1.61452850031306,330.352282187009));
#56175=CARTESIAN_POINT('Ctrl Pts',(109.364804973562,1.48380390032075,330.310915969201));
#56176=CARTESIAN_POINT('Ctrl Pts',(109.357047863787,1.35294054788719,330.269505844862));
#56177=CARTESIAN_POINT('Ctrl Pts',(109.349290754013,1.220411758324,330.233600026208));
#56178=CARTESIAN_POINT('Ctrl Pts',(109.341533644238,1.08672137685137,330.203311589065));
#56179=CARTESIAN_POINT('Ctrl Pts',(109.333772389312,0.952959555513651,330.173006966751));
#56180=CARTESIAN_POINT('Ctrl Pts',(109.326011134386,0.818035289730003,330.148325777502));
#56181=CARTESIAN_POINT('Ctrl Pts',(109.318249879459,0.68246030704377,330.129329513115));
#56182=CARTESIAN_POINT('Ctrl Pts',(109.310476209055,0.546668448568562,330.110302860896));
#56183=CARTESIAN_POINT('Ctrl Pts',(109.30270253865,0.410224182323015,330.096979344104));
#56184=CARTESIAN_POINT('Ctrl Pts',(109.294928868246,0.273642913204627,330.089368409405));
#56185=CARTESIAN_POINT('Ctrl Pts',(109.287517064068,0.143419535021954,330.082111765546));
#56186=CARTESIAN_POINT('Ctrl Pts',(109.280105259891,0.0130719096515187,
330.080047835702));
#56187=CARTESIAN_POINT('Ctrl Pts',(109.272693455714,-0.116957105141296,
330.083140829955));
#56188=CARTESIAN_POINT('Ctrl Pts',(109.264918376936,-0.253359229284194,
330.086385421069));
#56189=CARTESIAN_POINT('Ctrl Pts',(109.257143298157,-0.389841776951017,
330.095315484102));
#56190=CARTESIAN_POINT('Ctrl Pts',(109.249368219379,-0.525892041975531,
330.109946766886));
#56191=CARTESIAN_POINT('Ctrl Pts',(109.24160270833,-0.661774888487457,330.124560044946));
#56192=CARTESIAN_POINT('Ctrl Pts',(109.233837197281,-0.797226125869462,
330.144860542103));
#56193=CARTESIAN_POINT('Ctrl Pts',(109.226071686232,-0.931733040194316,
330.170812013981));
#56194=CARTESIAN_POINT('Ctrl Pts',(109.218313874709,-1.06610659052192,330.196737754899));
#56195=CARTESIAN_POINT('Ctrl Pts',(109.210556063187,-1.19953729975662,330.228303246762));
#56196=CARTESIAN_POINT('Ctrl Pts',(109.202798251665,-1.33151792579958,330.265420496414));
#56197=CARTESIAN_POINT('Ctrl Pts',(109.195046278142,-1.46339923223611,330.302509814159));
#56198=CARTESIAN_POINT('Ctrl Pts',(109.187294304619,-1.59383225276587,330.345142468445));
#56199=CARTESIAN_POINT('Ctrl Pts',(109.179542331096,-1.72232063948017,330.393179547961));
#56200=CARTESIAN_POINT('Ctrl Pts',(109.171793640538,-1.8507546112865,330.441196283746));
#56201=CARTESIAN_POINT('Ctrl Pts',(109.164044949981,-1.97724522190571,330.494612755949));
#56202=CARTESIAN_POINT('Ctrl Pts',(109.156296259423,-2.1013121905709,330.553240489946));
#56203=CARTESIAN_POINT('Ctrl Pts',(109.148549181045,-2.22535334606703,330.611856025953));
#56204=CARTESIAN_POINT('Ctrl Pts',(109.140802102668,-2.3469715094348,330.675680500215));
#56205=CARTESIAN_POINT('Ctrl Pts',(109.13305502429,-2.46570763317888,330.744477831078));
#56206=CARTESIAN_POINT('Ctrl Pts',(109.125307880984,-2.58444475204605,330.813275738529));
#56207=CARTESIAN_POINT('Ctrl Pts',(109.117560737678,-2.70029944490754,330.887046389749));
#56208=CARTESIAN_POINT('Ctrl Pts',(109.109813594372,-2.81283881983988,330.96550860255));
#56209=CARTESIAN_POINT('Ctrl Pts',(109.102064709344,-2.92540349601252,331.043988455321));
#56210=CARTESIAN_POINT('Ctrl Pts',(109.094315824316,-3.03465105050955,331.12716174503));
#56211=CARTESIAN_POINT('Ctrl Pts',(109.086566939288,-3.14017936760529,331.214705216002));
#56212=CARTESIAN_POINT('Ctrl Pts',(109.078809829513,-3.24581969354754,331.302341606518));
#56213=CARTESIAN_POINT('Ctrl Pts',(109.071052719739,-3.34773259500456,331.39435719429));
#56214=CARTESIAN_POINT('Ctrl Pts',(109.063295609964,-3.44555032454047,331.490389476942));
#56215=CARTESIAN_POINT('Ctrl Pts',(109.055534355038,-3.5434203247435,331.586473076175));
#56216=CARTESIAN_POINT('Ctrl Pts',(109.047773100111,-3.63719052550113,331.686577362048));
#56217=CARTESIAN_POINT('Ctrl Pts',(109.040011845185,-3.72653229191451,331.790305288689));
#56218=CARTESIAN_POINT('Ctrl Pts',(109.032238174781,-3.81601697603767,331.894199146208));
#56219=CARTESIAN_POINT('Ctrl Pts',(109.024464504376,-3.90105882718815,332.001727921166));
#56220=CARTESIAN_POINT('Ctrl Pts',(109.016690833971,-3.98137098630086,332.112463310719));
#56221=CARTESIAN_POINT('Ctrl Pts',(109.009279029794,-4.05794459508521,332.218043941249));
#56222=CARTESIAN_POINT('Ctrl Pts',(109.001867225617,-4.13021877715577,332.3265391294));
#56223=CARTESIAN_POINT('Ctrl Pts',(108.99445542144,-4.1979839732698,332.437557098652));
#56224=CARTESIAN_POINT('Ctrl Pts',(108.98643752161,-4.27129062592677,332.557653492927));
#56225=CARTESIAN_POINT('Ctrl Pts',(108.978419621781,-4.33954024120941,332.681062081186));
#56226=CARTESIAN_POINT('Ctrl Pts',(108.970401721951,-4.40243049178079,332.807332941932));
#56227=CARTESIAN_POINT('Ctrl Pts',(108.962395699245,-4.46522758138862,332.933416754368));
#56228=CARTESIAN_POINT('Ctrl Pts',(108.954389676539,-4.5226809591057,333.062354077842));
#56229=CARTESIAN_POINT('Ctrl Pts',(108.946383653833,-4.57453223890482,333.193667290414));
#56230=CARTESIAN_POINT('Ctrl Pts',(108.9383882249,-4.62631490776866,333.324806745995));
#56231=CARTESIAN_POINT('Ctrl Pts',(108.930392795968,-4.67251011317925,333.458315498203));
#56232=CARTESIAN_POINT('Ctrl Pts',(108.922397367035,-4.71290597159602,333.593692649029));
#56233=CARTESIAN_POINT('Ctrl Pts',(108.91441396919,-4.75324104451714,333.728866091665));
#56234=CARTESIAN_POINT('Ctrl Pts',(108.906430571345,-4.78779406588513,333.865901986915));
#56235=CARTESIAN_POINT('Ctrl Pts',(108.8984471735,-4.816401918241,334.004281352758));
#56236=CARTESIAN_POINT('Ctrl Pts',(108.890470898944,-4.84498424487213,334.14253724783));
#56237=CARTESIAN_POINT('Ctrl Pts',(108.882494624389,-4.86763189451933,334.282133877477));
#56238=CARTESIAN_POINT('Ctrl Pts',(108.874518349833,-4.88423188169256,334.42253832304));
#56239=CARTESIAN_POINT('Ctrl Pts',(108.866549434797,-4.90081655245036,334.562813220742));
#56240=CARTESIAN_POINT('Ctrl Pts',(108.858580519762,-4.91136464155386,334.703894094417));
#56241=CARTESIAN_POINT('Ctrl Pts',(108.850611604726,-4.91581450105162,334.845239366276));
#56242=CARTESIAN_POINT('Ctrl Pts',(108.84768019532,-4.91745140644305,334.897234005135));
#56243=CARTESIAN_POINT('Ctrl Pts',(108.844748785915,-4.91826361663179,334.949264349273));
#56244=CARTESIAN_POINT('Ctrl Pts',(108.841817376509,-4.91824982733319,335.001303240966));
#56245=CARTESIAN_POINT('',(107.091817376565,-4.9182483968572,335.00397105925));
#56246=CARTESIAN_POINT('Ctrl Pts',(108.84181737648,-4.91824982733305,335.001303241486));
#56247=CARTESIAN_POINT('Ctrl Pts',(108.833518067776,-4.91821078751442,335.148634018929));
#56248=CARTESIAN_POINT('Ctrl Pts',(108.825218759072,-4.91154738041952,335.295783482802));
#56249=CARTESIAN_POINT('Ctrl Pts',(108.816919450368,-4.89833361422636,335.442166107068));
#56250=CARTESIAN_POINT('Ctrl Pts',(108.808527611768,-4.88497252631503,335.590180767153));
#56251=CARTESIAN_POINT('Ctrl Pts',(108.800135773168,-4.86491422082103,335.737411076446));
#56252=CARTESIAN_POINT('Ctrl Pts',(108.791743934568,-4.83828747072515,335.88326519977));
#56253=CARTESIAN_POINT('Ctrl Pts',(108.783399897589,-4.81181239202047,336.028288508303));
#56254=CARTESIAN_POINT('Ctrl Pts',(108.775055860611,-4.77884366846353,336.171951004413));
#56255=CARTESIAN_POINT('Ctrl Pts',(108.766711823632,-4.7395575456705,336.313688446237));
#56256=CARTESIAN_POINT('Ctrl Pts',(108.758296084221,-4.69993382722955,336.456643873959));
#56257=CARTESIAN_POINT('Ctrl Pts',(108.74988034481,-4.6538837589856,336.597640722434));
#56258=CARTESIAN_POINT('Ctrl Pts',(108.741464605399,-4.60163695354992,336.736122233664));
#56259=CARTESIAN_POINT('Ctrl Pts',(108.733048865988,-4.54939014811427,336.874603744894));
#56260=CARTESIAN_POINT('Ctrl Pts',(108.724633126577,-4.49094678658842,337.010569666897));
#56261=CARTESIAN_POINT('Ctrl Pts',(108.716217387166,-4.42658291127038,337.143489396323));
#56262=CARTESIAN_POINT('Ctrl Pts',(108.708442308388,-4.36711883133142,337.266290414394));
#56263=CARTESIAN_POINT('Ctrl Pts',(108.700667229609,-4.30244684778947,337.386809153136));
#56264=CARTESIAN_POINT('Ctrl Pts',(108.692892150831,-4.23276504070697,337.504572453068));
#56265=CARTESIAN_POINT('Ctrl Pts',(108.685126639782,-4.16316898152424,337.622190837763));
#56266=CARTESIAN_POINT('Ctrl Pts',(108.677361128733,-4.08857556234406,337.737060197072));
#56267=CARTESIAN_POINT('Ctrl Pts',(108.669595617684,-4.00923018671835,337.848728904688));
#56268=CARTESIAN_POINT('Ctrl Pts',(108.661837806162,-3.92996348226347,337.960286892456));
#56269=CARTESIAN_POINT('Ctrl Pts',(108.654079994639,-3.84595442261319,338.068650227308));
#56270=CARTESIAN_POINT('Ctrl Pts',(108.646322183117,-3.75749324306918,338.173393702456));
#56271=CARTESIAN_POINT('Ctrl Pts',(108.638570209594,-3.66909863336823,338.278058354818));
#56272=CARTESIAN_POINT('Ctrl Pts',(108.630818236071,-3.57625882369179,338.379108272162));
#56273=CARTESIAN_POINT('Ctrl Pts',(108.623066262548,-3.47930587863644,338.476149258215));
#56274=CARTESIAN_POINT('Ctrl Pts',(108.615317571991,-3.38239399321076,338.573149147352));
#56275=CARTESIAN_POINT('Ctrl Pts',(108.607568881433,-3.28137271264234,338.666143206032));
#56276=CARTESIAN_POINT('Ctrl Pts',(108.599820190875,-3.17661255458554,338.754772395306));
#56277=CARTESIAN_POINT('Ctrl Pts',(108.592073112497,-3.0718741927546,338.843383144536));
#56278=CARTESIAN_POINT('Ctrl Pts',(108.58432603412,-2.96339879896313,338.92763057843));
#56279=CARTESIAN_POINT('Ctrl Pts',(108.576578955742,-2.85159142311456,339.007194706789));
#56280=CARTESIAN_POINT('Ctrl Pts',(108.568831812436,-2.73978311021256,339.086759501972));
#56281=CARTESIAN_POINT('Ctrl Pts',(108.56108466913,-2.62464307802337,339.161640686704));
#56282=CARTESIAN_POINT('Ctrl Pts',(108.553337525824,-2.5066065881345,339.231560761093));
#56283=CARTESIAN_POINT('Ctrl Pts',(108.545588640796,-2.38854356113689,339.301496554999));
#56284=CARTESIAN_POINT('Ctrl Pts',(108.537839755768,-2.26758311688829,339.366468819942));
#56285=CARTESIAN_POINT('Ctrl Pts',(108.53009087074,-2.1441860593072,339.426245497662));
#56286=CARTESIAN_POINT('Ctrl Pts',(108.522333760965,-2.0206580268141,339.486085622966));
#56287=CARTESIAN_POINT('Ctrl Pts',(108.514576651191,-1.89468856704656,339.540718974339));
#56288=CARTESIAN_POINT('Ctrl Pts',(108.506819541416,-1.76675996528577,339.589961033338));
#56289=CARTESIAN_POINT('Ctrl Pts',(108.49905828649,-1.63876300257057,339.639229405719));
#56290=CARTESIAN_POINT('Ctrl Pts',(108.491297031563,-1.50880518196739,339.683100620247));
#56291=CARTESIAN_POINT('Ctrl Pts',(108.483535776637,-1.37738402400586,339.721440067703));
#56292=CARTESIAN_POINT('Ctrl Pts',(108.475762106233,-1.24575263502173,339.75984084578));
#56293=CARTESIAN_POINT('Ctrl Pts',(108.467988435828,-1.11265361062778,339.7926920801));
#56294=CARTESIAN_POINT('Ctrl Pts',(108.460214765423,-0.97859561200515,339.819910133049));
#56295=CARTESIAN_POINT('Ctrl Pts',(108.452802961246,-0.85077804547189,339.845861179083));
#56296=CARTESIAN_POINT('Ctrl Pts',(108.445391157069,-0.722089060107164,
339.866691644544));
#56297=CARTESIAN_POINT('Ctrl Pts',(108.437979352892,-0.592972047854779,
339.882373112838));
#56298=CARTESIAN_POINT('Ctrl Pts',(108.430204274114,-0.457526626211204,
339.898823176606));
#56299=CARTESIAN_POINT('Ctrl Pts',(108.422429195335,-0.321182126475817,
339.909658730827));
#56300=CARTESIAN_POINT('Ctrl Pts',(108.414654116557,-0.184443631039657,
339.914790291505));
#56301=CARTESIAN_POINT('Ctrl Pts',(108.406888605508,-0.0478734010273303,
339.919915537471));
#56302=CARTESIAN_POINT('Ctrl Pts',(108.399123094459,0.0890894731342093,
339.919350741426));
#56303=CARTESIAN_POINT('Ctrl Pts',(108.39135758341,0.225932407303675,339.913057867543));
#56304=CARTESIAN_POINT('Ctrl Pts',(108.383599771888,0.362639661305597,339.906771233063));
#56305=CARTESIAN_POINT('Ctrl Pts',(108.375841960365,0.499226824028267,339.894767840924));
#56306=CARTESIAN_POINT('Ctrl Pts',(108.368084148843,0.635179267037453,339.877061652391));
#56307=CARTESIAN_POINT('Ctrl Pts',(108.36033217532,0.771029401521789,339.859368788327));
#56308=CARTESIAN_POINT('Ctrl Pts',(108.352580201797,0.90624538098487,339.835981720238));
#56309=CARTESIAN_POINT('Ctrl Pts',(108.344828228274,1.04031601816314,339.806966366104));
#56310=CARTESIAN_POINT('Ctrl Pts',(108.337079537716,1.17432987634696,339.77796329999));
#56311=CARTESIAN_POINT('Ctrl Pts',(108.329330847159,1.30719897574745,339.743336771115));
#56312=CARTESIAN_POINT('Ctrl Pts',(108.321582156601,1.43842088448955,339.703204059103));
#56313=CARTESIAN_POINT('Ctrl Pts',(108.313835078223,1.56961549141756,339.663079697037));
#56314=CARTESIAN_POINT('Ctrl Pts',(108.306087999846,1.69916321581614,339.617451544774));
#56315=CARTESIAN_POINT('Ctrl Pts',(108.298340921468,1.82657577535686,339.566487052361));
#56316=CARTESIAN_POINT('Ctrl Pts',(108.290593778162,1.95398940273756,339.515522132816));
#56317=CARTESIAN_POINT('Ctrl Pts',(108.282846634856,2.07926746664981,339.459220929084));
#56318=CARTESIAN_POINT('Ctrl Pts',(108.27509949155,2.20194106649374,339.397799290803));
#56319=CARTESIAN_POINT('Ctrl Pts',(108.267350606522,2.32464224596727,339.336363843634));
#56320=CARTESIAN_POINT('Ctrl Pts',(108.259601721494,2.44473744677209,339.269805846156));
#56321=CARTESIAN_POINT('Ctrl Pts',(108.251852836466,2.56178215872544,339.198387218175));
#56322=CARTESIAN_POINT('Ctrl Pts',(108.244095726691,2.67895110314544,339.126892785724));
#56323=CARTESIAN_POINT('Ctrl Pts',(108.236338616917,2.79306275667324,339.050527620855));
#56324=CARTESIAN_POINT('Ctrl Pts',(108.228581507142,2.90370096157295,338.96959743403));
#56325=CARTESIAN_POINT('Ctrl Pts',(108.220820252216,3.01439828799184,338.888624000702));
#56326=CARTESIAN_POINT('Ctrl Pts',(108.21305899729,3.12161816194648,338.803080928339));
#56327=CARTESIAN_POINT('Ctrl Pts',(108.205297742363,3.22497815076592,338.713313747798));
#56328=CARTESIAN_POINT('Ctrl Pts',(108.197524071959,3.32850348188246,338.623402969022));
#56329=CARTESIAN_POINT('Ctrl Pts',(108.189750401554,3.42815630499256,338.52925484776));
#56330=CARTESIAN_POINT('Ctrl Pts',(108.181976731149,3.52359102168934,338.431251866939));
#56331=CARTESIAN_POINT('Ctrl Pts',(108.174564926972,3.61458322936439,338.337810948452));
#56332=CARTESIAN_POINT('Ctrl Pts',(108.167153122795,3.70174100632332,338.24086619531));
#56333=CARTESIAN_POINT('Ctrl Pts',(108.159741318618,3.78480051162477,338.140775087412));
#56334=CARTESIAN_POINT('Ctrl Pts',(108.15196623984,3.87193101070197,338.035778216159));
#56335=CARTESIAN_POINT('Ctrl Pts',(108.144191161061,3.95482669166532,337.926986957682));
#56336=CARTESIAN_POINT('Ctrl Pts',(108.136416082283,4.03313897645041,337.814777621614));
#56337=CARTESIAN_POINT('Ctrl Pts',(108.128650571234,4.11135489298348,337.702706366277));
#56338=CARTESIAN_POINT('Ctrl Pts',(108.120885060185,4.18499841407718,337.587225719872));
#56339=CARTESIAN_POINT('Ctrl Pts',(108.113119549136,4.25376016590161,337.468746141969));
#56340=CARTESIAN_POINT('Ctrl Pts',(108.105361737613,4.32245374024891,337.350384036914));
#56341=CARTESIAN_POINT('Ctrl Pts',(108.097603926091,4.38627498283673,337.22902925358));
#56342=CARTESIAN_POINT('Ctrl Pts',(108.089846114569,4.44495713901647,337.105122109239));
#56343=CARTESIAN_POINT('Ctrl Pts',(108.082094141046,4.50359513501273,336.981308208954));
#56344=CARTESIAN_POINT('Ctrl Pts',(108.074342167523,4.55710157569387,336.854946122624));
#56345=CARTESIAN_POINT('Ctrl Pts',(108.066590194,4.60525526013601,336.726501390526));
#56346=CARTESIAN_POINT('Ctrl Pts',(108.058841503442,4.65338855146419,336.598111054849));
#56347=CARTESIAN_POINT('Ctrl Pts',(108.051092812885,4.69617345832183,336.467640192881));
#56348=CARTESIAN_POINT('Ctrl Pts',(108.043344122327,4.73343670892902,336.335574777039));
#56349=CARTESIAN_POINT('Ctrl Pts',(108.035597043949,4.77069220660572,336.20353683851));
#56350=CARTESIAN_POINT('Ctrl Pts',(108.027849965571,4.80242822705234,336.06990538195));
#56351=CARTESIAN_POINT('Ctrl Pts',(108.020102887194,4.8285213450012,335.935181631218));
#56352=CARTESIAN_POINT('Ctrl Pts',(108.012355743888,4.85461468163549,335.800456751371));
#56353=CARTESIAN_POINT('Ctrl Pts',(108.004608600582,4.87506494711981,335.664639942835));
#56354=CARTESIAN_POINT('Ctrl Pts',(107.996861457276,4.88979990500149,335.528242322753));
#56355=CARTESIAN_POINT('Ctrl Pts',(107.989112572248,4.90453817561453,335.39181403759));
#56356=CARTESIAN_POINT('Ctrl Pts',(107.98136368722,4.91355853979926,335.254805069582));
#56357=CARTESIAN_POINT('Ctrl Pts',(107.973614802192,4.91684070154239,335.11773095666));
#56358=CARTESIAN_POINT('Ctrl Pts',(107.965857692417,4.9201263470059,334.980511351859));
#56359=CARTESIAN_POINT('Ctrl Pts',(107.958100582642,4.91766161413682,334.843226855399));
#56360=CARTESIAN_POINT('Ctrl Pts',(107.950343472868,4.90947837455626,334.706392860672));
#56361=CARTESIAN_POINT('Ctrl Pts',(107.942582217941,4.90129076211412,334.569485746234));
#56362=CARTESIAN_POINT('Ctrl Pts',(107.934820963015,4.88737859365483,334.433030001873));
#56363=CARTESIAN_POINT('Ctrl Pts',(107.927059708089,4.86782547718353,334.297534209955));
#56364=CARTESIAN_POINT('Ctrl Pts',(107.919286037684,4.84824108209825,334.161821668929));
#56365=CARTESIAN_POINT('Ctrl Pts',(107.91151236728,4.82299777902962,334.027072533343));
#56366=CARTESIAN_POINT('Ctrl Pts',(107.903738696875,4.79223018290202,333.893784407729));
#56367=CARTESIAN_POINT('Ctrl Pts',(107.896326892698,4.76289482577666,333.766700876432));
#56368=CARTESIAN_POINT('Ctrl Pts',(107.888915088521,4.7285379888598,333.640945673746));
#56369=CARTESIAN_POINT('Ctrl Pts',(107.881503284344,4.68931750515014,333.516934122032));
#56370=CARTESIAN_POINT('Ctrl Pts',(107.873728205566,4.64817470870175,333.386844394757));
#56371=CARTESIAN_POINT('Ctrl Pts',(107.865953126787,4.60154942801112,333.25826245573));
#56372=CARTESIAN_POINT('Ctrl Pts',(107.858178048009,4.5495694742852,333.131685074418));
#56373=CARTESIAN_POINT('Ctrl Pts',(107.85041253696,4.49765348520154,333.005263454632));
#56374=CARTESIAN_POINT('Ctrl Pts',(107.842647025911,4.44039608089622,332.880841842581));
#56375=CARTESIAN_POINT('Ctrl Pts',(107.834881514862,4.37797500564806,332.758902520545));
#56376=CARTESIAN_POINT('Ctrl Pts',(107.827123703339,4.31561582107774,332.637084101701));
#56377=CARTESIAN_POINT('Ctrl Pts',(107.819365891817,4.2481033312079,332.517743420645));
#56378=CARTESIAN_POINT('Ctrl Pts',(107.811608080295,4.17566345197931,332.401343077991));
#56379=CARTESIAN_POINT('Ctrl Pts',(107.803856106772,4.10327808605705,332.285030330287));
#56380=CARTESIAN_POINT('Ctrl Pts',(107.796104133249,4.02597291709686,332.17165384724));
#56381=CARTESIAN_POINT('Ctrl Pts',(107.788352159726,3.94401972333747,332.061651571984));
#56382=CARTESIAN_POINT('Ctrl Pts',(107.780603469168,3.86210123680435,331.951695882757));
#56383=CARTESIAN_POINT('Ctrl Pts',(107.772854778611,3.77553887360009,331.845111871977));
#56384=CARTESIAN_POINT('Ctrl Pts',(107.765106088053,3.68464753099484,331.74230823514));
#56385=CARTESIAN_POINT('Ctrl Pts',(107.757359009675,3.59377509909251,331.639525987459));
#56386=CARTESIAN_POINT('Ctrl Pts',(107.749611931298,3.49857573804616,331.540522841892));
#56387=CARTESIAN_POINT('Ctrl Pts',(107.74186485292,3.39940414519525,331.445673830368));
#56388=CARTESIAN_POINT('Ctrl Pts',(107.734117709614,3.30023172119101,331.350824023918));
#56389=CARTESIAN_POINT('Ctrl Pts',(107.726370566308,3.19708728145803,331.26012869112));
#56390=CARTESIAN_POINT('Ctrl Pts',(107.718623423002,3.09036154401724,331.17392517196));
#56391=CARTESIAN_POINT('Ctrl Pts',(107.710874537974,2.98361181236482,331.08770227242));
#56392=CARTESIAN_POINT('Ctrl Pts',(107.703125652946,2.8732794848576,331.005973441574));
#56393=CARTESIAN_POINT('Ctrl Pts',(107.695376767918,2.7597871050036,330.929034733929));
#56394=CARTESIAN_POINT('Ctrl Pts',(107.687619658143,2.64617426316494,330.852014362745));
#56395=CARTESIAN_POINT('Ctrl Pts',(107.679862548369,2.52939499287368,330.77979449078));
#56396=CARTESIAN_POINT('Ctrl Pts',(107.672105438594,2.40989994699168,330.712627225446));
#56397=CARTESIAN_POINT('Ctrl Pts',(107.664344183668,2.29034104677787,330.645424068072));
#56398=CARTESIAN_POINT('Ctrl Pts',(107.656582928742,2.16806382755665,330.58327907423));
#56399=CARTESIAN_POINT('Ctrl Pts',(107.648821673815,2.043541212177,330.526397159265));
#56400=CARTESIAN_POINT('Ctrl Pts',(107.641048003411,1.91881940119457,330.469424251773));
#56401=CARTESIAN_POINT('Ctrl Pts',(107.633274333006,1.79184537858289,330.417731394696));
#56402=CARTESIAN_POINT('Ctrl Pts',(107.625500662601,1.66311043846837,330.371474669837));
#56403=CARTESIAN_POINT('Ctrl Pts',(107.618088858424,1.54036814078723,330.327371206649));
#56404=CARTESIAN_POINT('Ctrl Pts',(107.610677054247,1.4160254521268,330.288209247777));
#56405=CARTESIAN_POINT('Ctrl Pts',(107.60326525007,1.29051703841253,330.254080822847));
#56406=CARTESIAN_POINT('Ctrl Pts',(107.595490171292,1.1588570834726,330.218279662148));
#56407=CARTESIAN_POINT('Ctrl Pts',(107.587715092513,1.02549817302981,330.18790479015));
#56408=CARTESIAN_POINT('Ctrl Pts',(107.579940013735,0.890927217104305,330.163117558145));
#56409=CARTESIAN_POINT('Ctrl Pts',(107.572174502686,0.756521859307278,330.138360828408));
#56410=CARTESIAN_POINT('Ctrl Pts',(107.564408991637,0.62090780441603,330.11917812763));
#56411=CARTESIAN_POINT('Ctrl Pts',(107.556643480588,0.484586801516951,330.10568097747));
#56412=CARTESIAN_POINT('Ctrl Pts',(107.548885669066,0.348400961289134,330.092197209775));
#56413=CARTESIAN_POINT('Ctrl Pts',(107.541127857543,0.211509954432455,330.084387812536));
#56414=CARTESIAN_POINT('Ctrl Pts',(107.533370046021,0.074425047752714,330.082313147956));
#56415=CARTESIAN_POINT('Ctrl Pts',(107.525618072498,-0.0625566981874454,
330.080240044627));
#56416=CARTESIAN_POINT('Ctrl Pts',(107.517866098975,-0.199731664256605,
330.083893089921));
#56417=CARTESIAN_POINT('Ctrl Pts',(107.510114125452,-0.336584499931678,
330.093280735878));
#56418=CARTESIAN_POINT('Ctrl Pts',(107.502365434895,-0.473379378349593,
330.102664406161));
#56419=CARTESIAN_POINT('Ctrl Pts',(107.494616744337,-0.609852008561665,
330.117777820084));
#56420=CARTESIAN_POINT('Ctrl Pts',(107.486868053779,-0.745488300824605,
330.138577342399));
#56421=CARTESIAN_POINT('Ctrl Pts',(107.479120975402,-0.881096372824082,
330.1593725372));
#56422=CARTESIAN_POINT('Ctrl Pts',(107.471373897024,-1.01586806687144,330.185851428027));
#56423=CARTESIAN_POINT('Ctrl Pts',(107.463626818646,-1.14929606353317,330.217918693618));
#56424=CARTESIAN_POINT('Ctrl Pts',(107.45587967534,-1.28272517845002,330.249986227963));
#56425=CARTESIAN_POINT('Ctrl Pts',(107.448132532034,-1.414810193467,330.287642139151));
#56426=CARTESIAN_POINT('Ctrl Pts',(107.440385388728,-1.54505599225037,330.330740418084));
#56427=CARTESIAN_POINT('Ctrl Pts',(107.4326365037,-1.67533107305451,330.373848386426));
#56428=CARTESIAN_POINT('Ctrl Pts',(107.424887618672,-1.80376574380302,330.422401034494));
#56429=CARTESIAN_POINT('Ctrl Pts',(107.417138733644,-1.92988238340716,330.476203248518));
#56430=CARTESIAN_POINT('Ctrl Pts',(107.409381623869,-2.0561328845156,330.530062568769));
#56431=CARTESIAN_POINT('Ctrl Pts',(107.401624514095,-2.18006007954213,330.589182431838));
#56432=CARTESIAN_POINT('Ctrl Pts',(107.39386740432,-2.30120809186383,330.653320303905));
#56433=CARTESIAN_POINT('Ctrl Pts',(107.386106149394,-2.42242084180975,330.717492449201));
#56434=CARTESIAN_POINT('Ctrl Pts',(107.378344894468,-2.54085111252258,330.786687749468));
#56435=CARTESIAN_POINT('Ctrl Pts',(107.370583639541,-2.65607066062768,330.860619405243));
#56436=CARTESIAN_POINT('Ctrl Pts',(107.362809969137,-2.77147452245979,330.934669327573));
#56437=CARTESIAN_POINT('Ctrl Pts',(107.355036298732,-2.88365707819748,331.013470520959));
#56438=CARTESIAN_POINT('Ctrl Pts',(107.347262628327,-2.99222120788063,331.096694310509));
#56439=CARTESIAN_POINT('Ctrl Pts',(107.33985082415,-3.09573165120778,331.176044012634));
#56440=CARTESIAN_POINT('Ctrl Pts',(107.332439019973,-3.19595274152198,331.259413649204));
#56441=CARTESIAN_POINT('Ctrl Pts',(107.325027215796,-3.29257186647513,331.346487502882));
#56442=CARTESIAN_POINT('Ctrl Pts',(107.317367950252,-3.39241685927191,331.436468531974));
#56443=CARTESIAN_POINT('Ctrl Pts',(107.309708684708,-3.4887509638778,331.530708390154));
#56444=CARTESIAN_POINT('Ctrl Pts',(107.302049419163,-3.5811807498019,331.628898177191));
#56445=CARTESIAN_POINT('Ctrl Pts',(107.294399665406,-3.67349575025715,331.726966025605));
#56446=CARTESIAN_POINT('Ctrl Pts',(107.286749911648,-3.76191580043934,331.828973757283));
#56447=CARTESIAN_POINT('Ctrl Pts',(107.27910015789,-3.84608082321445,331.934572564258));
#56448=CARTESIAN_POINT('Ctrl Pts',(107.271296708668,-3.93193685234707,332.042293015688));
#56449=CARTESIAN_POINT('Ctrl Pts',(107.263493259446,-4.01336470738464,332.153750130447));
#56450=CARTESIAN_POINT('Ctrl Pts',(107.255689810224,-4.09002141961977,332.268533754638));
#56451=CARTESIAN_POINT('Ctrl Pts',(107.24805347621,-4.16503648570301,332.380859223641));
#56452=CARTESIAN_POINT('Ctrl Pts',(107.240417142196,-4.23548245496336,332.496369811835));
#56453=CARTESIAN_POINT('Ctrl Pts',(107.232780808182,-4.30107893507099,332.614648232065));
#56454=CARTESIAN_POINT('Ctrl Pts',(107.225147462329,-4.36664974672413,332.732880368955));
#56455=CARTESIAN_POINT('Ctrl Pts',(107.217514116477,-4.42737464720835,332.853877831972));
#56456=CARTESIAN_POINT('Ctrl Pts',(107.209880770624,-4.48301770655805,332.977196177286));
#56457=CARTESIAN_POINT('Ctrl Pts',(107.202248645274,-4.53865186909091,333.100494805123));
#56458=CARTESIAN_POINT('Ctrl Pts',(107.194616519924,-4.58920564146773,333.226113209185));
#56459=CARTESIAN_POINT('Ctrl Pts',(107.186984394574,-4.63449026864816,333.35358479954));
#56460=CARTESIAN_POINT('Ctrl Pts',(107.179053809739,-4.68154578215933,333.486041253655));
#56461=CARTESIAN_POINT('Ctrl Pts',(107.171123224905,-4.72291148549212,333.620498350175));
#56462=CARTESIAN_POINT('Ctrl Pts',(107.163192640071,-4.75843206096906,333.756413499735));
#56463=CARTESIAN_POINT('Ctrl Pts',(107.155554518819,-4.79264271101794,333.887316379417));
#56464=CARTESIAN_POINT('Ctrl Pts',(107.147916397567,-4.82143164608762,334.019571264848));
#56465=CARTESIAN_POINT('Ctrl Pts',(107.140278276315,-4.8447121656197,334.152682412081));
#56466=CARTESIAN_POINT('Ctrl Pts',(107.132636775724,-4.86800298516572,334.285852451758));
#56467=CARTESIAN_POINT('Ctrl Pts',(107.124995275133,-4.88578048327286,334.419879108267));
#56468=CARTESIAN_POINT('Ctrl Pts',(107.117353774543,-4.89800980322335,334.554261253616));
#56469=CARTESIAN_POINT('Ctrl Pts',(107.109704288804,-4.91025190246137,334.688783824441));
#56470=CARTESIAN_POINT('Ctrl Pts',(107.102054803065,-4.91693423712501,334.823662223669));
#56471=CARTESIAN_POINT('Ctrl Pts',(107.094405317326,-4.91807402271891,334.958395077725));
#56472=CARTESIAN_POINT('Ctrl Pts',(107.093542670405,-4.91820255848797,334.973589155548));
#56473=CARTESIAN_POINT('Ctrl Pts',(107.092680023485,-4.91826066120041,334.988781387545));
#56474=CARTESIAN_POINT('Ctrl Pts',(107.091817376565,-4.9182483968572,335.00397105925));
#56475=CARTESIAN_POINT('',(105.341817376472,-4.91824882476302,334.996599968063));
#56476=CARTESIAN_POINT('Ctrl Pts',(107.091817376509,-4.91824839685641,335.003971060231));
#56477=CARTESIAN_POINT('Ctrl Pts',(107.079247665722,-4.91806969189428,335.225301219511));
#56478=CARTESIAN_POINT('Ctrl Pts',(107.066677954934,-4.90294797263902,335.446045535405));
#56479=CARTESIAN_POINT('Ctrl Pts',(107.054108244147,-4.87313418658796,335.664639949151));
#56480=CARTESIAN_POINT('Ctrl Pts',(107.051668556606,-4.86734755206395,335.707067501934));
#56481=CARTESIAN_POINT('Ctrl Pts',(107.049228869064,-4.86100754838075,335.749414178383));
#56482=CARTESIAN_POINT('Ctrl Pts',(107.046789181522,-4.85411616778059,335.791668675767));
#56483=CARTESIAN_POINT('Ctrl Pts',(107.039014102744,-4.83215391804811,335.926330201189));
#56484=CARTESIAN_POINT('Ctrl Pts',(107.031239023965,-4.80454910457406,336.060289919449));
#56485=CARTESIAN_POINT('Ctrl Pts',(107.023463945187,-4.77135660038552,336.19303782608));
#56486=CARTESIAN_POINT('Ctrl Pts',(107.015698434138,-4.73820494168652,336.32562237796));
#56487=CARTESIAN_POINT('Ctrl Pts',(107.007932923089,-4.69947936746907,336.456997709719));
#56488=CARTESIAN_POINT('Ctrl Pts',(107.00016741204,-4.65528625056723,336.586660955523));
#56489=CARTESIAN_POINT('Ctrl Pts',(106.992409600518,-4.61113695126951,336.71619563984));
#56490=CARTESIAN_POINT('Ctrl Pts',(106.984651788995,-4.56153102283847,336.844021248808));
#56491=CARTESIAN_POINT('Ctrl Pts',(106.976893977473,-4.50662534362196,336.969647449348));
#56492=CARTESIAN_POINT('Ctrl Pts',(106.96914200395,-4.45176098267015,337.095179112189));
#56493=CARTESIAN_POINT('Ctrl Pts',(106.961390030427,-4.39160496521674,337.218514304329));
#56494=CARTESIAN_POINT('Ctrl Pts',(106.953638056904,-4.32636310708101,337.339180482175));
#56495=CARTESIAN_POINT('Ctrl Pts',(106.945889366347,-4.26114887891098,337.459795557823));
#56496=CARTESIAN_POINT('Ctrl Pts',(106.938140675789,-4.1908532794453,337.577743524203));
#56497=CARTESIAN_POINT('Ctrl Pts',(106.930391985231,-4.11572900897169,337.692574564837));
#56498=CARTESIAN_POINT('Ctrl Pts',(106.922644906853,-4.04062036873001,337.807381713915));
#56499=CARTESIAN_POINT('Ctrl Pts',(106.914897828476,-3.96068526964706,337.919072900274));
#56500=CARTESIAN_POINT('Ctrl Pts',(106.907150750098,-3.87622064867957,338.02722588276));
#56501=CARTESIAN_POINT('Ctrl Pts',(106.899403606792,-3.79175531981721,338.135379771671));
#56502=CARTESIAN_POINT('Ctrl Pts',(106.891656463486,-3.70276063393929,338.239995089502));
#56503=CARTESIAN_POINT('Ctrl Pts',(106.88390932018,-3.60957460539302,338.34068170148));
#56504=CARTESIAN_POINT('Ctrl Pts',(106.876160435152,-3.5163676266492,338.441390949945));
#56505=CARTESIAN_POINT('Ctrl Pts',(106.868411550124,-3.41896769560604,338.538169448164));
#56506=CARTESIAN_POINT('Ctrl Pts',(106.860662665096,-3.31775027058181,338.63066332845));
#56507=CARTESIAN_POINT('Ctrl Pts',(106.852905555321,-3.21642541233688,338.723255382697));
#56508=CARTESIAN_POINT('Ctrl Pts',(106.845148445547,-3.11127525500551,338.811553470386));
#56509=CARTESIAN_POINT('Ctrl Pts',(106.837391335772,-3.00270940718991,338.895243160378));
#56510=CARTESIAN_POINT('Ctrl Pts',(106.829630080846,-2.89408554525651,338.978977571465));
#56511=CARTESIAN_POINT('Ctrl Pts',(106.82186882592,-2.78204267501926,339.058098452584));
#56512=CARTESIAN_POINT('Ctrl Pts',(106.814107570993,-2.66701924469968,339.132334861903));
#56513=CARTESIAN_POINT('Ctrl Pts',(106.806333900589,-2.55181181437772,339.206690025284));
#56514=CARTESIAN_POINT('Ctrl Pts',(106.798560230184,-2.4336146334237,339.276144904922));
#56515=CARTESIAN_POINT('Ctrl Pts',(106.790786559779,-2.31289136828018,339.340474234578));
#56516=CARTESIAN_POINT('Ctrl Pts',(106.783374755602,-2.19778780017286,339.401809018462));
#56517=CARTESIAN_POINT('Ctrl Pts',(106.775962951425,-2.0803882929454,339.458484577115));
#56518=CARTESIAN_POINT('Ctrl Pts',(106.768551147248,-1.96110970855013,339.51034718991));
#56519=CARTESIAN_POINT('Ctrl Pts',(106.76077606847,-1.83598492542161,339.564751743848));
#56520=CARTESIAN_POINT('Ctrl Pts',(106.753000989691,-1.70839679189643,339.614031557433));
#56521=CARTESIAN_POINT('Ctrl Pts',(106.745225910913,-1.57880387655637,339.657956781881));
#56522=CARTESIAN_POINT('Ctrl Pts',(106.737460399864,-1.44937043354892,339.701827953544));
#56523=CARTESIAN_POINT('Ctrl Pts',(106.729694888815,-1.31793748402125,339.74035752234));
#56524=CARTESIAN_POINT('Ctrl Pts',(106.721929377766,-1.18498546302489,339.773362809898));
#56525=CARTESIAN_POINT('Ctrl Pts',(106.714171566244,-1.05216526434435,339.806335372618));
#56526=CARTESIAN_POINT('Ctrl Pts',(106.706413754722,-0.91782936846196,339.833794460748));
#56527=CARTESIAN_POINT('Ctrl Pts',(106.698655943199,-0.782475002798547,
339.855606649276));
#56528=CARTESIAN_POINT('Ctrl Pts',(106.690903969676,-0.64722249558772,339.877402423441));
#56529=CARTESIAN_POINT('Ctrl Pts',(106.683151996153,-0.510953428480875,
339.89355969443));
#56530=CARTESIAN_POINT('Ctrl Pts',(106.67540002263,-0.374176552216034,339.903995816706));
#56531=CARTESIAN_POINT('Ctrl Pts',(106.667651332073,-0.237457601039497,
339.914427519278));
#56532=CARTESIAN_POINT('Ctrl Pts',(106.659902641515,-0.100231657369472,
339.919142862458));
#56533=CARTESIAN_POINT('Ctrl Pts',(106.652153950958,0.0369862678958382,
339.918110925801));
#56534=CARTESIAN_POINT('Ctrl Pts',(106.64440687258,0.174175643825637,339.917079203848));
#56535=CARTESIAN_POINT('Ctrl Pts',(106.636659794202,0.311356614051241,339.910302583467));
#56536=CARTESIAN_POINT('Ctrl Pts',(106.628912715824,0.448013417350148,339.897802266361));
#56537=CARTESIAN_POINT('Ctrl Pts',(106.621165572518,0.58467136596469,339.885301844491));
#56538=CARTESIAN_POINT('Ctrl Pts',(106.613418429213,0.720804749641099,339.867077665822));
#56539=CARTESIAN_POINT('Ctrl Pts',(106.605671285907,0.855902576767339,339.843202849518));
#56540=CARTESIAN_POINT('Ctrl Pts',(106.597922400879,0.991030776753234,339.819322665649));
#56541=CARTESIAN_POINT('Ctrl Pts',(106.590173515851,1.12512257207817,339.789789384234));
#56542=CARTESIAN_POINT('Ctrl Pts',(106.582424630823,1.25767720581652,339.754727238073));
#56543=CARTESIAN_POINT('Ctrl Pts',(106.574667521048,1.39037253441276,339.719627876587));
#56544=CARTESIAN_POINT('Ctrl Pts',(106.566910411273,1.52152706375457,339.678988027799));
#56545=CARTESIAN_POINT('Ctrl Pts',(106.559153301499,1.65065471927012,339.632981983588));
#56546=CARTESIAN_POINT('Ctrl Pts',(106.551392046572,1.77985137647608,339.586951355218));
#56547=CARTESIAN_POINT('Ctrl Pts',(106.543630791646,1.90701863948305,339.535548964035));
#56548=CARTESIAN_POINT('Ctrl Pts',(106.53586953672,2.03169139803317,339.478996888329));
#56549=CARTESIAN_POINT('Ctrl Pts',(106.528095866315,2.15656359236621,339.422354347732));
#56550=CARTESIAN_POINT('Ctrl Pts',(106.520322195911,2.27893295917535,339.360545837333));
#56551=CARTESIAN_POINT('Ctrl Pts',(106.512548525506,2.39835915075817,339.293839359649));
#56552=CARTESIAN_POINT('Ctrl Pts',(106.505136721329,2.51222602439118,339.23023808455));
#56553=CARTESIAN_POINT('Ctrl Pts',(106.497724917152,2.62341732052589,339.162184731144));
#56554=CARTESIAN_POINT('Ctrl Pts',(106.490313112975,2.73157818428538,339.089946660488));
#56555=CARTESIAN_POINT('Ctrl Pts',(106.482538034196,2.84504033417182,339.014167986803));
#56556=CARTESIAN_POINT('Ctrl Pts',(106.474762955418,2.95552604080997,338.933544538154));
#56557=CARTESIAN_POINT('Ctrl Pts',(106.46698787664,3.0625938616824,338.848337550279));
#56558=CARTESIAN_POINT('Ctrl Pts',(106.459222365591,3.16952992878496,338.763235415026));
#56559=CARTESIAN_POINT('Ctrl Pts',(106.451456854542,3.27305617578858,338.673561204271));
#56560=CARTESIAN_POINT('Ctrl Pts',(106.443691343493,3.3727589935798,338.579620068349));
#56561=CARTESIAN_POINT('Ctrl Pts',(106.43593353197,3.47236295573698,338.485772075336));
#56562=CARTESIAN_POINT('Ctrl Pts',(106.428175720448,3.56815075021403,338.387665842748));
#56563=CARTESIAN_POINT('Ctrl Pts',(106.420417908926,3.65974109878217,338.285647295798));
#56564=CARTESIAN_POINT('Ctrl Pts',(106.412665935403,3.7512625227084,338.18370552104));
#56565=CARTESIAN_POINT('Ctrl Pts',(106.40491396188,3.83859252791289,338.077857581773));
#56566=CARTESIAN_POINT('Ctrl Pts',(106.397161988357,3.921386301782,337.968486573104));
#56567=CARTESIAN_POINT('Ctrl Pts',(106.389413297799,4.00414501243878,337.859161883121));
#56568=CARTESIAN_POINT('Ctrl Pts',(106.381664607242,4.0823710772588,337.746317402262));
#56569=CARTESIAN_POINT('Ctrl Pts',(106.373915916684,4.1557597926331,337.630369481353));
#56570=CARTESIAN_POINT('Ctrl Pts',(106.366168838306,4.22913323887222,337.514445684377));
#56571=CARTESIAN_POINT('Ctrl Pts',(106.358421759928,4.29767112865233,337.395420061756));
#56572=CARTESIAN_POINT('Ctrl Pts',(106.350674681551,4.36111218294644,337.273737801563));
#56573=CARTESIAN_POINT('Ctrl Pts',(106.342927538245,4.42455376893765,337.152054521555));
#56574=CARTESIAN_POINT('Ctrl Pts',(106.335180394939,4.48289825353818,337.027714906162));
#56575=CARTESIAN_POINT('Ctrl Pts',(106.327433251633,4.53593059733132,336.901188228107));
#56576=CARTESIAN_POINT('Ctrl Pts',(106.319684366605,4.58897486392122,336.774633104169));
#56577=CARTESIAN_POINT('Ctrl Pts',(106.311935481577,4.6367044621499,336.645890299564));
#56578=CARTESIAN_POINT('Ctrl Pts',(106.304186596549,4.67895287372387,336.515448140971));
#56579=CARTESIAN_POINT('Ctrl Pts',(106.296429486774,4.72124612819842,336.384867529722));
#56580=CARTESIAN_POINT('Ctrl Pts',(106.288672376999,4.75804645381128,336.252584333846));
#56581=CARTESIAN_POINT('Ctrl Pts',(106.280915267225,4.78923737348115,336.119101623156));
#56582=CARTESIAN_POINT('Ctrl Pts',(106.273154012298,4.82044496058119,335.985547583574));
#56583=CARTESIAN_POINT('Ctrl Pts',(106.265392757372,4.846037096082,335.850793135779));
#56584=CARTESIAN_POINT('Ctrl Pts',(106.257631502446,4.86594883250799,335.715349580215));
#56585=CARTESIAN_POINT('Ctrl Pts',(106.249857832041,4.88589242122303,335.579689359104));
#56586=CARTESIAN_POINT('Ctrl Pts',(106.242084161637,4.90013741213522,335.44333821637));
#56587=CARTESIAN_POINT('Ctrl Pts',(106.234310491232,4.90867087686924,335.30681148133));
#56588=CARTESIAN_POINT('Ctrl Pts',(106.226898687055,4.91680710676677,335.176640098654));
#56589=CARTESIAN_POINT('Ctrl Pts',(106.219486882878,4.91975158052645,335.046309391145));
#56590=CARTESIAN_POINT('Ctrl Pts',(106.212075078701,4.91753709542967,334.91626244825));
#56591=CARTESIAN_POINT('Ctrl Pts',(106.204299999923,4.91521407182167,334.779841517292));
#56592=CARTESIAN_POINT('Ctrl Pts',(106.196524921144,4.90720624935718,334.643301755234));
#56593=CARTESIAN_POINT('Ctrl Pts',(106.188749842366,4.89349441686567,334.507155750156));
#56594=CARTESIAN_POINT('Ctrl Pts',(106.180984331317,4.87979945765698,334.371177281404));
#56595=CARTESIAN_POINT('Ctrl Pts',(106.173218820268,4.86041449330612,334.235591990719));
#56596=CARTESIAN_POINT('Ctrl Pts',(106.165453309219,4.83537230361631,334.100912825183));
#56597=CARTESIAN_POINT('Ctrl Pts',(106.157695497697,4.81035494333049,333.966367194432));
#56598=CARTESIAN_POINT('Ctrl Pts',(106.149937686174,4.77969159123611,333.832726282726));
#56599=CARTESIAN_POINT('Ctrl Pts',(106.142179874652,4.74346681169933,333.700497915043));
#56600=CARTESIAN_POINT('Ctrl Pts',(106.134427901129,4.70726929245792,333.568369053401));
#56601=CARTESIAN_POINT('Ctrl Pts',(106.126675927606,4.66551877897275,333.43765099543));
#56602=CARTESIAN_POINT('Ctrl Pts',(106.118923954083,4.61835082620066,333.308841016157));
#56603=CARTESIAN_POINT('Ctrl Pts',(106.111175263526,4.57120284908455,333.180085587988));
#56604=CARTESIAN_POINT('Ctrl Pts',(106.103426572968,4.51864212998409,333.053236997593));
#56605=CARTESIAN_POINT('Ctrl Pts',(106.09567788241,4.46085389458412,332.928776788061));
#56606=CARTESIAN_POINT('Ctrl Pts',(106.087930804032,4.40307768250918,332.804342473516));
#56607=CARTESIAN_POINT('Ctrl Pts',(106.080183725655,4.34007628201017,332.682295905719));
#56608=CARTESIAN_POINT('Ctrl Pts',(106.072436647277,4.27208266816222,332.56309771659));
#56609=CARTESIAN_POINT('Ctrl Pts',(106.064689503971,4.20408848446235,332.443898528466));
#56610=CARTESIAN_POINT('Ctrl Pts',(106.056942360665,4.13110219763241,332.327548106146));
#56611=CARTESIAN_POINT('Ctrl Pts',(106.049195217359,4.05340205894974,332.21448123126));
#56612=CARTESIAN_POINT('Ctrl Pts',(106.041446332331,3.97568445162629,332.10138893654));
#56613=CARTESIAN_POINT('Ctrl Pts',(106.033697447303,3.89325110495208,331.991581980291));
#56614=CARTESIAN_POINT('Ctrl Pts',(106.025948562275,3.8064225506459,331.885464652884));
#56615=CARTESIAN_POINT('Ctrl Pts',(106.0181914525,3.71950183561507,331.779234691449));
#56616=CARTESIAN_POINT('Ctrl Pts',(106.010434342726,3.6281768418562,331.676702484844));
#56617=CARTESIAN_POINT('Ctrl Pts',(106.002677232951,3.53280757907679,331.578238221074));
#56618=CARTESIAN_POINT('Ctrl Pts',(105.994915978025,3.43738735401274,331.47972134115));
#56619=CARTESIAN_POINT('Ctrl Pts',(105.987154723099,3.33791883699792,331.385277004513));
#56620=CARTESIAN_POINT('Ctrl Pts',(105.979393468173,3.23479684467875,331.295236520889));
#56621=CARTESIAN_POINT('Ctrl Pts',(105.971619797768,3.13150989077918,331.205052001835));
#56622=CARTESIAN_POINT('Ctrl Pts',(105.963846127363,3.02455808789032,331.119285657913));
#56623=CARTESIAN_POINT('Ctrl Pts',(105.956072456959,2.91436779114319,331.038227235132));
#56624=CARTESIAN_POINT('Ctrl Pts',(105.948660652781,2.80930687921841,330.960942101432));
#56625=CARTESIAN_POINT('Ctrl Pts',(105.941248848604,2.70130243049351,330.887936606421));
#56626=CARTESIAN_POINT('Ctrl Pts',(105.933837044427,2.59074479682716,330.819422951289));
#56627=CARTESIAN_POINT('Ctrl Pts',(105.926061965649,2.47476840420195,330.747551237827));
#56628=CARTESIAN_POINT('Ctrl Pts',(105.91828688687,2.35561571311514,330.680395686678));
#56629=CARTESIAN_POINT('Ctrl Pts',(105.910511808092,2.23370737355073,330.618249843744));
#56630=CARTESIAN_POINT('Ctrl Pts',(105.902746297043,2.1119490499593,330.556180475228));
#56631=CARTESIAN_POINT('Ctrl Pts',(105.894980785994,1.98744216991709,330.499108724638));
#56632=CARTESIAN_POINT('Ctrl Pts',(105.887215274945,1.86063582060239,330.44728461184));
#56633=CARTESIAN_POINT('Ctrl Pts',(105.879457463422,1.73395520015223,330.3955118828));
#56634=CARTESIAN_POINT('Ctrl Pts',(105.8716996519,1.60498000711307,330.348976584112));
#56635=CARTESIAN_POINT('Ctrl Pts',(105.863941840378,1.47418304497533,330.307882417031));
#56636=CARTESIAN_POINT('Ctrl Pts',(105.856189866855,1.34348451169958,330.266819174614));
#56637=CARTESIAN_POINT('Ctrl Pts',(105.848437893332,1.21096730951346,330.231189030343));
#56638=CARTESIAN_POINT('Ctrl Pts',(105.840685919809,1.07712296416119,330.201147097214));
#56639=CARTESIAN_POINT('Ctrl Pts',(105.832937229251,0.943335301968555,330.171117886861));
#56640=CARTESIAN_POINT('Ctrl Pts',(105.825188538694,0.808221995071072,330.146672266054));
#56641=CARTESIAN_POINT('Ctrl Pts',(105.817439848136,0.672288219570297,330.127915065157));
#56642=CARTESIAN_POINT('Ctrl Pts',(105.809692769758,0.536382726226855,330.109161766852));
#56643=CARTESIAN_POINT('Ctrl Pts',(105.80194569138,0.39965749078738,330.096094587742));
#56644=CARTESIAN_POINT('Ctrl Pts',(105.794198613003,0.262625944641374,330.088766888479));
#56645=CARTESIAN_POINT('Ctrl Pts',(105.786451469697,0.125593250039026,330.081439127803));
#56646=CARTESIAN_POINT('Ctrl Pts',(105.778704326391,-0.0117453700736549,
330.079850963789));
#56647=CARTESIAN_POINT('Ctrl Pts',(105.770957183085,-0.148873720815505,
330.08400369429));
#56648=CARTESIAN_POINT('Ctrl Pts',(105.763208298057,-0.286032900921733,
330.088157358414));
#56649=CARTESIAN_POINT('Ctrl Pts',(105.755459413029,-0.422981326970275,
330.098054473522));
#56650=CARTESIAN_POINT('Ctrl Pts',(105.747710528001,-0.559205564457357,
330.113644282374));
#56651=CARTESIAN_POINT('Ctrl Pts',(105.739953418226,-0.695574391757753,
330.129250638409));
#56652=CARTESIAN_POINT('Ctrl Pts',(105.732196308451,-0.8312171060709,330.150561713703));
#56653=CARTESIAN_POINT('Ctrl Pts',(105.724439198677,-0.965627586495292,
330.177475098385));
#56654=CARTESIAN_POINT('Ctrl Pts',(105.716677943751,-1.10010989158272,330.204402864718));
#56655=CARTESIAN_POINT('Ctrl Pts',(105.708916688824,-1.23335827120195,330.236938812974));
#56656=CARTESIAN_POINT('Ctrl Pts',(105.701155433898,-1.36488046199348,330.274930224116));
#56657=CARTESIAN_POINT('Ctrl Pts',(105.693381763494,-1.4966130454273,330.312982409135));
#56658=CARTESIAN_POINT('Ctrl Pts',(105.685608093089,-1.62661355121246,330.356507371933));
#56659=CARTESIAN_POINT('Ctrl Pts',(105.677834422684,-1.75440760052237,330.405303379577));
#56660=CARTESIAN_POINT('Ctrl Pts',(105.670422618507,-1.87625280609057,330.451827921325));
#56661=CARTESIAN_POINT('Ctrl Pts',(105.66301081433,-1.99609208884605,330.503143704025));
#56662=CARTESIAN_POINT('Ctrl Pts',(105.655599010153,-2.11353576249201,330.559037306713));
#56663=CARTESIAN_POINT('Ctrl Pts',(105.647823931375,-2.23673570043089,330.617670421367));
#56664=CARTESIAN_POINT('Ctrl Pts',(105.640048852596,-2.35768859422035,330.681526739201));
#56665=CARTESIAN_POINT('Ctrl Pts',(105.632273773818,-2.47591995700338,330.750411381203));
#56666=CARTESIAN_POINT('Ctrl Pts',(105.624508262769,-2.59400582856752,330.819211256266));
#56667=CARTESIAN_POINT('Ctrl Pts',(105.61674275172,-2.70937649820478,330.893026948911));
#56668=CARTESIAN_POINT('Ctrl Pts',(105.608977240671,-2.8215786920368,330.971616112243));
#56669=CARTESIAN_POINT('Ctrl Pts',(105.601219429149,-2.93366963706683,331.050127354189));
#56670=CARTESIAN_POINT('Ctrl Pts',(105.593461617626,-3.0425980400692,331.133402425266));
#56671=CARTESIAN_POINT('Ctrl Pts',(105.585703806104,-3.14793674321381,331.221153969368));
#56672=CARTESIAN_POINT('Ctrl Pts',(105.577951832581,-3.2531961756439,331.30883947765));
#56673=CARTESIAN_POINT('Ctrl Pts',(105.570199859058,-3.35487098603542,331.400994504577));
#56674=CARTESIAN_POINT('Ctrl Pts',(105.562447885535,-3.45256474377734,331.497289656205));
#56675=CARTESIAN_POINT('Ctrl Pts',(105.554699194978,-3.55021712815485,331.59354402678));
#56676=CARTESIAN_POINT('Ctrl Pts',(105.54695050442,-3.64389153537855,331.693934760958));
#56677=CARTESIAN_POINT('Ctrl Pts',(105.539201813862,-3.73322643158218,331.798093775103));
#56678=CARTESIAN_POINT('Ctrl Pts',(105.531454735485,-3.82254274091457,331.902231118095));
#56679=CARTESIAN_POINT('Ctrl Pts',(105.523707657107,-3.9075210807928,332.01013488507));
#56680=CARTESIAN_POINT('Ctrl Pts',(105.515960578729,-3.98783873192088,332.121402197129));
#56681=CARTESIAN_POINT('Ctrl Pts',(105.508213435423,-4.06815705618808,332.232670441716));
#56682=CARTESIAN_POINT('Ctrl Pts',(105.500466292117,-4.14381438502051,332.347301970683));
#56683=CARTESIAN_POINT('Ctrl Pts',(105.492719148811,-4.2145302843566,332.464863407084));
#56684=CARTESIAN_POINT('Ctrl Pts',(105.484970263783,-4.28526208212835,332.582451273793));
#56685=CARTESIAN_POINT('Ctrl Pts',(105.477221378755,-4.35105003832197,332.702970023805));
#56686=CARTESIAN_POINT('Ctrl Pts',(105.469472493727,-4.41165898691453,332.825960431437));
#56687=CARTESIAN_POINT('Ctrl Pts',(105.461715383952,-4.47233226647129,332.949081382359));
#56688=CARTESIAN_POINT('Ctrl Pts',(105.453958274178,-4.52781538449648,333.074678880306));
#56689=CARTESIAN_POINT('Ctrl Pts',(105.446201164403,-4.5779205685756,333.202271897557));
#56690=CARTESIAN_POINT('Ctrl Pts',(105.438439909477,-4.628052527263,333.329933096437));
#56691=CARTESIAN_POINT('Ctrl Pts',(105.43067865455,-4.67280069825269,333.459591570102));
#56692=CARTESIAN_POINT('Ctrl Pts',(105.422917399624,-4.7120271142913,333.590750718757));
#56693=CARTESIAN_POINT('Ctrl Pts',(105.41514372922,-4.75131627981175,333.722119679305));
#56694=CARTESIAN_POINT('Ctrl Pts',(105.407370058815,-4.78506594313833,333.854993732891));
#56695=CARTESIAN_POINT('Ctrl Pts',(105.39959638841,-4.81318903219623,333.988864794973));
#56696=CARTESIAN_POINT('Ctrl Pts',(105.392184584233,-4.84000298469279,334.116504126908));
#56697=CARTESIAN_POINT('Ctrl Pts',(105.384772780056,-4.86170236052158,334.245049450957));
#56698=CARTESIAN_POINT('Ctrl Pts',(105.377360975879,-4.87825574831046,334.374057577268));
#56699=CARTESIAN_POINT('Ctrl Pts',(105.365513109422,-4.90471655639987,334.58027876388));
#56700=CARTESIAN_POINT('Ctrl Pts',(105.353665242965,-4.9181047645561,334.788212569106));
#56701=CARTESIAN_POINT('Ctrl Pts',(105.341817376508,-4.91824882476258,334.996599967431));
#56702=CARTESIAN_POINT('',(103.591817376553,-4.91824952580637,334.997840276541));
#56703=CARTESIAN_POINT('Ctrl Pts',(105.341817376472,-4.91824882476302,334.996599968063));
#56704=CARTESIAN_POINT('Ctrl Pts',(105.334158591598,-4.91834194920273,335.13130728099));
#56705=CARTESIAN_POINT('Ctrl Pts',(105.326499806723,-4.91289660595529,335.266230429205));
#56706=CARTESIAN_POINT('Ctrl Pts',(105.318841021849,-4.90188611779449,335.400868495487));
#56707=CARTESIAN_POINT('Ctrl Pts',(105.31119031737,-4.89088724624152,335.535364511971));
#56708=CARTESIAN_POINT('Ctrl Pts',(105.303539612892,-4.87433493981361,335.669575646368));
#56709=CARTESIAN_POINT('Ctrl Pts',(105.295888908413,-4.85225454198551,335.802999951607));
#56710=CARTESIAN_POINT('Ctrl Pts',(105.288244324432,-4.83019180828679,335.936317518543));
#56711=CARTESIAN_POINT('Ctrl Pts',(105.280599740452,-4.80260984610632,336.068849112915));
#56712=CARTESIAN_POINT('Ctrl Pts',(105.272955156471,-4.76958586071718,336.200097404275));
#56713=CARTESIAN_POINT('Ctrl Pts',(105.265314147281,-4.73657731813556,336.331284320786));
#56714=CARTESIAN_POINT('Ctrl Pts',(105.257673138092,-4.69813190983903,336.461188737582));
#56715=CARTESIAN_POINT('Ctrl Pts',(105.250032128902,-4.65437795177756,336.589323423507));
#56716=CARTESIAN_POINT('Ctrl Pts',(105.242392815477,-4.61063370401019,336.717429672565));
#56717=CARTESIAN_POINT('Ctrl Pts',(105.234753502053,-4.56158337873665,336.843766590538));
#56718=CARTESIAN_POINT('Ctrl Pts',(105.227114188628,-4.50740502695809,336.967862542317));
#56719=CARTESIAN_POINT('Ctrl Pts',(105.219474808225,-4.45322620016345,337.091959582124));
#56720=CARTESIAN_POINT('Ctrl Pts',(105.211835427822,-4.39391941889369,337.213815247516));
#56721=CARTESIAN_POINT('Ctrl Pts',(105.204196047419,-4.32971047981391,337.332978830485));
#56722=CARTESIAN_POINT('Ctrl Pts',(105.196554837451,-4.26548616325695,337.452170952086));
#56723=CARTESIAN_POINT('Ctrl Pts',(105.188913627483,-4.19635754581876,337.568669354893));
#56724=CARTESIAN_POINT('Ctrl Pts',(105.181272417516,-4.12259559524014,337.682049332247));
#56725=CARTESIAN_POINT('Ctrl Pts',(105.173623269308,-4.04875701543377,337.795547096889));
#56726=CARTESIAN_POINT('Ctrl Pts',(105.165974121101,-3.97027571268535,337.905919630354));
#56727=CARTESIAN_POINT('Ctrl Pts',(105.158324972894,-3.88746524452945,338.012772317165));
#56728=CARTESIAN_POINT('Ctrl Pts',(105.150671437674,-3.80460728211723,338.119686287157));
#56729=CARTESIAN_POINT('Ctrl Pts',(105.143017902454,-3.71741547073258,338.223076084499));
#56730=CARTESIAN_POINT('Ctrl Pts',(105.135364367234,-3.62624172249859,338.322582434269));
#56731=CARTESIAN_POINT('Ctrl Pts',(105.127699536033,-3.53493340940863,338.42223564712));
#56732=CARTESIAN_POINT('Ctrl Pts',(105.120034704833,-3.43963170969533,338.517993684794));
#56733=CARTESIAN_POINT('Ctrl Pts',(105.112369873632,-3.34072353461826,338.609535888137));
#56734=CARTESIAN_POINT('Ctrl Pts',(105.107954229623,-3.28374337689356,338.662272572247));
#56735=CARTESIAN_POINT('Ctrl Pts',(105.103538585614,-3.22556689088289,338.713610864243));
#56736=CARTESIAN_POINT('Ctrl Pts',(105.099122941605,-3.16627243683877,338.763495970267));
#56737=CARTESIAN_POINT('Ctrl Pts',(105.091347862826,-3.06186659018059,338.85133380964));
#56738=CARTESIAN_POINT('Ctrl Pts',(105.083572784048,-2.95363783367437,338.934962561326));
#56739=CARTESIAN_POINT('Ctrl Pts',(105.07579770527,-2.84196011347315,339.014031112975));
#56740=CARTESIAN_POINT('Ctrl Pts',(105.068032194221,-2.73041981981638,339.093002365737));
#56741=CARTESIAN_POINT('Ctrl Pts',(105.060266683172,-2.61543932310731,339.167424360266));
#56742=CARTESIAN_POINT('Ctrl Pts',(105.052501172122,-2.49742698350977,339.236984956846));
#56743=CARTESIAN_POINT('Ctrl Pts',(105.0447433606,-2.37953165349075,339.306476583891));
#56744=CARTESIAN_POINT('Ctrl Pts',(105.036985549078,-2.25861079741665,339.371116208037));
#56745=CARTESIAN_POINT('Ctrl Pts',(105.029227737556,-2.13510292039348,339.430634106065));
#56746=CARTESIAN_POINT('Ctrl Pts',(105.021475764033,-2.01168798696383,339.490107214988));
#56747=CARTESIAN_POINT('Ctrl Pts',(105.01372379051,-1.88569025832933,339.544466100508));
#56748=CARTESIAN_POINT('Ctrl Pts',(105.005971816987,-1.757573769774,339.593486421696));
#56749=CARTESIAN_POINT('Ctrl Pts',(104.998223126429,-1.62951153862798,339.642485982748));
#56750=CARTESIAN_POINT('Ctrl Pts',(104.990474435872,-1.49933269652401,339.686151336816));
#56751=CARTESIAN_POINT('Ctrl Pts',(104.982725745314,-1.36752203421418,339.724305932985));
#56752=CARTESIAN_POINT('Ctrl Pts',(104.974978666936,-1.23573879621356,339.762452590772));
#56753=CARTESIAN_POINT('Ctrl Pts',(104.967231588558,-1.10232478854908,339.795090662633));
#56754=CARTESIAN_POINT('Ctrl Pts',(104.95948451018,-0.967780389813594,339.822093339992));
#56755=CARTESIAN_POINT('Ctrl Pts',(104.951737366875,-0.833234863466634,
339.849096243659));
#56756=CARTESIAN_POINT('Ctrl Pts',(104.943990223569,-0.697559310384833,
339.870463581708));
#56757=CARTESIAN_POINT('Ctrl Pts',(104.936243080263,-0.56126434803956,339.886119666373));
#56758=CARTESIAN_POINT('Ctrl Pts',(104.928494195235,-0.424938743693313,
339.901779270859));
#56759=CARTESIAN_POINT('Ctrl Pts',(104.920745310207,-0.287993841223883,
339.911725022325));
#56760=CARTESIAN_POINT('Ctrl Pts',(104.912996425179,-0.150945029684462,
339.915933142397));
#56761=CARTESIAN_POINT('Ctrl Pts',(104.905239315404,-0.0137507531200268,
339.92014572901));
#56762=CARTESIAN_POINT('Ctrl Pts',(104.897482205629,0.123547261522099,339.918608506904));
#56763=CARTESIAN_POINT('Ctrl Pts',(104.889725095855,0.260433417295594,339.911349865124));
#56764=CARTESIAN_POINT('Ctrl Pts',(104.881963840928,0.397392720653963,339.904087344558));
#56765=CARTESIAN_POINT('Ctrl Pts',(104.874202586002,0.533939337686005,339.891097349283));
#56766=CARTESIAN_POINT('Ctrl Pts',(104.866441331076,0.669564132802064,339.872460049561));
#56767=CARTESIAN_POINT('Ctrl Pts',(104.858667660671,0.805405883390107,339.853792936233));
#56768=CARTESIAN_POINT('Ctrl Pts',(104.850893990267,0.940322480474719,339.829460535569));
#56769=CARTESIAN_POINT('Ctrl Pts',(104.843120319862,1.07381542145992,339.799594097748));
#56770=CARTESIAN_POINT('Ctrl Pts',(104.835708515685,1.20109423392509,339.771117949793));
#56771=CARTESIAN_POINT('Ctrl Pts',(104.828296711508,1.32707867176214,339.737611462832));
#56772=CARTESIAN_POINT('Ctrl Pts',(104.820884907331,1.45135235581407,339.699229660463));
#56773=CARTESIAN_POINT('Ctrl Pts',(104.813109828553,1.58171706331423,339.658966651626));
#56774=CARTESIAN_POINT('Ctrl Pts',(104.805334749774,1.71061105505814,339.613211097475));
#56775=CARTESIAN_POINT('Ctrl Pts',(104.797559670996,1.8375367094602,339.562087450267));
#56776=CARTESIAN_POINT('Ctrl Pts',(104.789794159947,1.96430617376386,339.511026713963));
#56777=CARTESIAN_POINT('Ctrl Pts',(104.782028648898,2.0891117610358,339.454611172852));
#56778=CARTESIAN_POINT('Ctrl Pts',(104.774263137849,2.21146999921276,339.393015308997));
#56779=CARTESIAN_POINT('Ctrl Pts',(104.766505326326,2.33370691884083,339.33148051762));
#56780=CARTESIAN_POINT('Ctrl Pts',(104.758747514804,2.45350097147044,339.26477579966));
#56781=CARTESIAN_POINT('Ctrl Pts',(104.750989703282,2.57038804081908,339.193123940705));
#56782=CARTESIAN_POINT('Ctrl Pts',(104.743237729759,2.68718714894094,339.121526002046));
#56783=CARTESIAN_POINT('Ctrl Pts',(104.735485756236,2.80108329618332,339.044988536062));
#56784=CARTESIAN_POINT('Ctrl Pts',(104.727733782713,2.91163671335181,338.96378035617));
#56785=CARTESIAN_POINT('Ctrl Pts',(104.719985092155,3.02214331108264,338.882606567991));
#56786=CARTESIAN_POINT('Ctrl Pts',(104.712236401598,3.12930968000112,338.796766231026));
#56787=CARTESIAN_POINT('Ctrl Pts',(104.70448771104,3.23272500658261,338.70657147433));
#56788=CARTESIAN_POINT('Ctrl Pts',(104.696740632662,3.33611881674152,338.616395483406));
#56789=CARTESIAN_POINT('Ctrl Pts',(104.688993554284,3.43576284251314,338.521867131554));
#56790=CARTESIAN_POINT('Ctrl Pts',(104.681246475907,3.53127966429302,338.423338574411));
#56791=CARTESIAN_POINT('Ctrl Pts',(104.673499332601,3.62679728659593,338.324809191504));
#56792=CARTESIAN_POINT('Ctrl Pts',(104.665752189295,3.71818736384754,338.222279817082));
#56793=CARTESIAN_POINT('Ctrl Pts',(104.658005045989,3.80510992417901,338.116138881278));
#56794=CARTESIAN_POINT('Ctrl Pts',(104.650256160961,3.89205202654741,338.009974082739));
#56795=CARTESIAN_POINT('Ctrl Pts',(104.642507275933,3.97452436576206,337.900196409467));
#56796=CARTESIAN_POINT('Ctrl Pts',(104.634758390905,4.05222803948967,337.787226395267));
#56797=CARTESIAN_POINT('Ctrl Pts',(104.62700128113,4.13001418869945,337.674136473527));
#56798=CARTESIAN_POINT('Ctrl Pts',(104.619244171355,4.20302133971685,337.557847764803));
#56799=CARTESIAN_POINT('Ctrl Pts',(104.611487061581,4.27099434640244,337.438809208507));
#56800=CARTESIAN_POINT('Ctrl Pts',(104.603725806654,4.33900367568931,337.319707041813));
#56801=CARTESIAN_POINT('Ctrl Pts',(104.595964551728,4.40197332105235,337.197852446648));
#56802=CARTESIAN_POINT('Ctrl Pts',(104.588203296802,4.45969517689283,337.073716950719));
#56803=CARTESIAN_POINT('Ctrl Pts',(104.580429626398,4.51750936889123,336.949382878452));
#56804=CARTESIAN_POINT('Ctrl Pts',(104.572655955993,4.57005884625894,336.822760975452));
#56805=CARTESIAN_POINT('Ctrl Pts',(104.564882285588,4.61718421171329,336.69434147019));
#56806=CARTESIAN_POINT('Ctrl Pts',(104.557470481411,4.66211588006781,336.571899923794));
#56807=CARTESIAN_POINT('Ctrl Pts',(104.550058677234,4.70211696865175,336.44782463956));
#56808=CARTESIAN_POINT('Ctrl Pts',(104.542646873057,4.73709251346281,336.322549651769));
#56809=CARTESIAN_POINT('Ctrl Pts',(104.534871794279,4.77378231391201,336.191134563651));
#56810=CARTESIAN_POINT('Ctrl Pts',(104.5270967155,4.80505742714246,336.057983900356));
#56811=CARTESIAN_POINT('Ctrl Pts',(104.519321636722,4.83075321612019,335.923583470751));
#56812=CARTESIAN_POINT('Ctrl Pts',(104.511556125673,4.85641738479367,335.789348429431));
#56813=CARTESIAN_POINT('Ctrl Pts',(104.503790614624,4.87651581731665,335.653867062066));
#56814=CARTESIAN_POINT('Ctrl Pts',(104.496025103575,4.89093360490284,335.517640352882));
#56815=CARTESIAN_POINT('Ctrl Pts',(104.488267292052,4.9053370972107,335.381548712877));
#56816=CARTESIAN_POINT('Ctrl Pts',(104.48050948053,4.91407111245435,335.244713587923));
#56817=CARTESIAN_POINT('Ctrl Pts',(104.472751669008,4.91707183583693,335.107645825368));
#56818=CARTESIAN_POINT('Ctrl Pts',(104.464999695485,4.92007030107998,334.970681210653));
#56819=CARTESIAN_POINT('Ctrl Pts',(104.457247721962,4.91734405371076,334.833484696006));
#56820=CARTESIAN_POINT('Ctrl Pts',(104.449495748439,4.90888116032316,334.696571563092));
#56821=CARTESIAN_POINT('Ctrl Pts',(104.441747057881,4.90042185097591,334.559716412971));
#56822=CARTESIAN_POINT('Ctrl Pts',(104.433998367324,4.88623075172543,334.423144795204));
#56823=CARTESIAN_POINT('Ctrl Pts',(104.426249676766,4.86634802378248,334.28737108259));
#56824=CARTESIAN_POINT('Ctrl Pts',(104.418502598388,4.84646943260715,334.151625618832));
#56825=CARTESIAN_POINT('Ctrl Pts',(104.410755520011,4.82090162477888,334.016678116525));
#56826=CARTESIAN_POINT('Ctrl Pts',(104.403008441633,4.78973649208191,333.883036527491));
#56827=CARTESIAN_POINT('Ctrl Pts',(104.395261298327,4.7585710981911,333.749393818412));
#56828=CARTESIAN_POINT('Ctrl Pts',(104.387514155021,4.72180837463398,333.617057425095));
#56829=CARTESIAN_POINT('Ctrl Pts',(104.379767011715,4.67959098231029,333.486523438972));
#56830=CARTESIAN_POINT('Ctrl Pts',(104.372018126687,4.63736409862057,333.355960106038));
#56831=CARTESIAN_POINT('Ctrl Pts',(104.364269241659,4.58968022617278,333.227200358473));
#56832=CARTESIAN_POINT('Ctrl Pts',(104.356520356631,4.53673124761302,333.100723124599));
#56833=CARTESIAN_POINT('Ctrl Pts',(104.348763246856,4.4837260684603,332.974111646483));
#56834=CARTESIAN_POINT('Ctrl Pts',(104.341006137082,4.42544477094841,332.849787882718));
#56835=CARTESIAN_POINT('Ctrl Pts',(104.333249027307,4.36212680359099,332.728209338013));
#56836=CARTESIAN_POINT('Ctrl Pts',(104.325487772381,4.29877500113634,332.606565825621));
#56837=CARTESIAN_POINT('Ctrl Pts',(104.317726517455,4.23038136071163,332.487670793977));
#56838=CARTESIAN_POINT('Ctrl Pts',(104.309965262529,4.1572297821454,332.371954414219));
#56839=CARTESIAN_POINT('Ctrl Pts',(104.302191592124,4.0839611848935,332.256052925965));
#56840=CARTESIAN_POINT('Ctrl Pts',(104.294417921719,4.00591966279319,332.143340572076));
#56841=CARTESIAN_POINT('Ctrl Pts',(104.286644251315,3.92343120040872,332.034216683883));
#56842=CARTESIAN_POINT('Ctrl Pts',(104.279232447137,3.84478259579287,331.930172538937));
#56843=CARTESIAN_POINT('Ctrl Pts',(104.27182064296,3.76209192654405,331.829390514423));
#56844=CARTESIAN_POINT('Ctrl Pts',(104.264408838783,3.67567279087798,331.732185348448));
#56845=CARTESIAN_POINT('Ctrl Pts',(104.256633760005,3.5850179959445,331.63021586773));
#56846=CARTESIAN_POINT('Ctrl Pts',(104.248858681226,3.48997352086974,331.531860493697));
#56847=CARTESIAN_POINT('Ctrl Pts',(104.241083602448,3.39085879814743,331.437520572196));
#56848=CARTESIAN_POINT('Ctrl Pts',(104.233318091399,3.2918660424014,331.343296741974));
#56849=CARTESIAN_POINT('Ctrl Pts',(104.22555258035,3.18881328530124,331.253078799483));
#56850=CARTESIAN_POINT('Ctrl Pts',(104.217787069301,3.08205963143479,331.167234485286));
#56851=CARTESIAN_POINT('Ctrl Pts',(104.210029257778,2.97541182412724,331.081475285976));
#56852=CARTESIAN_POINT('Ctrl Pts',(104.202271446256,2.86507072511024,331.000081328516));
#56853=CARTESIAN_POINT('Ctrl Pts',(104.194513634734,2.75143138296973,330.923382724941));
#56854=CARTESIAN_POINT('Ctrl Pts',(104.186761661211,2.63787755803828,330.846741839498));
#56855=CARTESIAN_POINT('Ctrl Pts',(104.179009687688,2.52103075302939,330.774789492663));
#56856=CARTESIAN_POINT('Ctrl Pts',(104.171257714165,2.40131782143594,330.707814567967));
#56857=CARTESIAN_POINT('Ctrl Pts',(104.163509023608,2.28165558833945,330.640868007191));
#56858=CARTESIAN_POINT('Ctrl Pts',(104.15576033305,2.15912998324193,330.578894866453));
#56859=CARTESIAN_POINT('Ctrl Pts',(104.148011642492,2.03419528673923,330.522139729971));
#56860=CARTESIAN_POINT('Ctrl Pts',(104.140264564115,1.90928658394378,330.465396401868));
#56861=CARTESIAN_POINT('Ctrl Pts',(104.132517485737,1.78197014237945,330.413869080152));
#56862=CARTESIAN_POINT('Ctrl Pts',(104.124770407359,1.65272283748507,330.367755372937));
#56863=CARTESIAN_POINT('Ctrl Pts',(104.117023264053,1.5234744493737,330.321641279244));
#56864=CARTESIAN_POINT('Ctrl Pts',(104.109276120747,1.39229553379929,330.280941021897));
#56865=CARTESIAN_POINT('Ctrl Pts',(104.101528977441,1.25968046662818,330.245803097841));
#56866=CARTESIAN_POINT('Ctrl Pts',(104.093780092413,1.12703558477439,330.210657274034));
#56867=CARTESIAN_POINT('Ctrl Pts',(104.086031207385,0.992954286596443,330.181076372026));
#56868=CARTESIAN_POINT('Ctrl Pts',(104.078282322357,0.857943151847668,330.157158209202));
#56869=CARTESIAN_POINT('Ctrl Pts',(104.070525212582,0.722788714885544,330.133214659394));
#56870=CARTESIAN_POINT('Ctrl Pts',(104.062768102808,0.586702855340249,330.114945923579));
#56871=CARTESIAN_POINT('Ctrl Pts',(104.055010993033,0.450199878011816,330.102398226444));
#56872=CARTESIAN_POINT('Ctrl Pts',(104.047249738107,0.313623957856817,330.089843824221));
#56873=CARTESIAN_POINT('Ctrl Pts',(104.039488483181,0.176630865973257,330.083016571751));
#56874=CARTESIAN_POINT('Ctrl Pts',(104.031727228254,0.0397359769346117,
330.081910521896));
#56875=CARTESIAN_POINT('Ctrl Pts',(104.02395355785,-0.097377899312462,330.080802702722));
#56876=CARTESIAN_POINT('Ctrl Pts',(104.016179887445,-0.234392867940548,
330.085434361476));
#56877=CARTESIAN_POINT('Ctrl Pts',(104.008406217041,-0.370796713761589,
330.095747471881));
#56878=CARTESIAN_POINT('Ctrl Pts',(104.000994412863,-0.500850927742978,
330.105580504515));
#56879=CARTESIAN_POINT('Ctrl Pts',(103.993582608686,-0.630349348166679,
330.120577916078));
#56880=CARTESIAN_POINT('Ctrl Pts',(103.986170804509,-0.758857599052846,
330.14064631799));
#56881=CARTESIAN_POINT('Ctrl Pts',(103.978395725731,-0.893664422121261,
330.161698332061));
#56882=CARTESIAN_POINT('Ctrl Pts',(103.970620646952,-1.02780757357939,330.188397522317));
#56883=CARTESIAN_POINT('Ctrl Pts',(103.962845568174,-1.16077668989048,330.220692462426));
#56884=CARTESIAN_POINT('Ctrl Pts',(103.955080057125,-1.29358217923854,330.252947661556));
#56885=CARTESIAN_POINT('Ctrl Pts',(103.947314546076,-1.42521613182715,330.290784818149));
#56886=CARTESIAN_POINT('Ctrl Pts',(103.939549035027,-1.55517497467427,330.334100959017));
#56887=CARTESIAN_POINT('Ctrl Pts',(103.931791223505,-1.68500496295034,330.377374151805));
#56888=CARTESIAN_POINT('Ctrl Pts',(103.924033411983,-1.81316277829227,330.426115395226));
#56889=CARTESIAN_POINT('Ctrl Pts',(103.91627560046,-1.93915703898772,330.480171127062));
#56890=CARTESIAN_POINT('Ctrl Pts',(103.908523626937,-2.06505648500657,330.534186180245));
#56891=CARTESIAN_POINT('Ctrl Pts',(103.900771653414,-2.18879525935524,330.593507607898));
#56892=CARTESIAN_POINT('Ctrl Pts',(103.893019679891,-2.30989943879194,330.657932791265));
#56893=CARTESIAN_POINT('Ctrl Pts',(103.885270989334,-2.43095233053667,330.722330690529));
#56894=CARTESIAN_POINT('Ctrl Pts',(103.877522298776,-2.54937250215816,330.791827863354));
#56895=CARTESIAN_POINT('Ctrl Pts',(103.869773608219,-2.66470844027314,330.866174654048));
#56896=CARTESIAN_POINT('Ctrl Pts',(103.862026529841,-2.78002038178296,330.940505976271));
#56897=CARTESIAN_POINT('Ctrl Pts',(103.854279451463,-2.89224903784756,331.019684697742));
#56898=CARTESIAN_POINT('Ctrl Pts',(103.846532373085,-3.00097017092505,331.10341674082));
#56899=CARTESIAN_POINT('Ctrl Pts',(103.838785229779,-3.1096922151902,331.187149485654));
#56900=CARTESIAN_POINT('Ctrl Pts',(103.831038086473,-3.2149063681568,331.275435389709));
#56901=CARTESIAN_POINT('Ctrl Pts',(103.823290943168,-3.3162202204275,331.367939081991));
#56902=CARTESIAN_POINT('Ctrl Pts',(103.81554205814,-3.41755685020343,331.460463571067));
#56903=CARTESIAN_POINT('Ctrl Pts',(103.807793173111,-3.51499114581035,331.557207471776));
#56904=CARTESIAN_POINT('Ctrl Pts',(103.800044288083,-3.60816671115022,331.657797724995));
#56905=CARTESIAN_POINT('Ctrl Pts',(103.792287178309,-3.70144117399769,331.758494745748));
#56906=CARTESIAN_POINT('Ctrl Pts',(103.784530068534,-3.79044761089548,331.863045987095));
#56907=CARTESIAN_POINT('Ctrl Pts',(103.776772958759,-3.87486883068108,331.971043973988));
#56908=CARTESIAN_POINT('Ctrl Pts',(103.769011703833,-3.95933516246709,332.079099671551));
#56909=CARTESIAN_POINT('Ctrl Pts',(103.761250448907,-4.03921116740232,332.190605467076));
#56910=CARTESIAN_POINT('Ctrl Pts',(103.753489193981,-4.11422294780748,332.305124752751));
#56911=CARTESIAN_POINT('Ctrl Pts',(103.745715523576,-4.1893547226151,332.419827231962));
#56912=CARTESIAN_POINT('Ctrl Pts',(103.737941853171,-4.25960652339841,332.537552498484));
#56913=CARTESIAN_POINT('Ctrl Pts',(103.730168182767,-4.3247499566633,332.657838418289));
#56914=CARTESIAN_POINT('Ctrl Pts',(103.72275637859,-4.3868609474371,332.772524999589));
#56915=CARTESIAN_POINT('Ctrl Pts',(103.715344574412,-4.44432833000703,332.889538943999));
#56916=CARTESIAN_POINT('Ctrl Pts',(103.707932770235,-4.49699557105443,333.008464437572));
#56917=CARTESIAN_POINT('Ctrl Pts',(103.69938140188,-4.5577603953395,333.145674714325));
#56918=CARTESIAN_POINT('Ctrl Pts',(103.690830033525,-4.6123013316562,333.285802805362));
#56919=CARTESIAN_POINT('Ctrl Pts',(103.682278665169,-4.66035602045924,333.42829238563));
#56920=CARTESIAN_POINT('Ctrl Pts',(103.673760056184,-4.70822661693014,333.570236103677));
#56921=CARTESIAN_POINT('Ctrl Pts',(103.665241447199,-4.74966043838958,333.714523022454));
#56922=CARTESIAN_POINT('Ctrl Pts',(103.656722838214,-4.7844438726408,333.860579141823));
#56923=CARTESIAN_POINT('Ctrl Pts',(103.648225198979,-4.81914168259438,334.006275723586));
#56924=CARTESIAN_POINT('Ctrl Pts',(103.639727559743,-4.84722168144211,334.153732572376));
#56925=CARTESIAN_POINT('Ctrl Pts',(103.631229920508,-4.86851934992104,334.302359403457));
#56926=CARTESIAN_POINT('Ctrl Pts',(103.62276552463,-4.88973370043676,334.450404796019));
#56927=CARTESIAN_POINT('Ctrl Pts',(103.614301128751,-4.90421858397522,334.599610788059));
#56928=CARTESIAN_POINT('Ctrl Pts',(103.605836732873,-4.91186026695796,334.749377214963));
#56929=CARTESIAN_POINT('Ctrl Pts',(103.601163614099,-4.91607917315269,334.83206194654));
#56930=CARTESIAN_POINT('Ctrl Pts',(103.596490495326,-4.91821311226992,334.914917225596));
#56931=CARTESIAN_POINT('Ctrl Pts',(103.591817376553,-4.91824952580637,334.997840276542));
#56932=CARTESIAN_POINT('',(101.841817376472,-4.91824811790539,335.004302699158));
#56933=CARTESIAN_POINT('Ctrl Pts',(103.591817376509,-4.91824952580671,334.997840277318));
#56934=CARTESIAN_POINT('Ctrl Pts',(103.583929525821,-4.91831098892144,335.137807754317));
#56935=CARTESIAN_POINT('Ctrl Pts',(103.576041675134,-4.91239314012991,335.277751606086));
#56936=CARTESIAN_POINT('Ctrl Pts',(103.568153824446,-4.90052846099034,335.417137705708));
#56937=CARTESIAN_POINT('Ctrl Pts',(103.560262823948,-4.88865904399659,335.556579465581));
#56938=CARTESIAN_POINT('Ctrl Pts',(103.552371823451,-4.87083809652471,335.695462660097));
#56939=CARTESIAN_POINT('Ctrl Pts',(103.544480822953,-4.84714990479059,335.833259181161));
#56940=CARTESIAN_POINT('Ctrl Pts',(103.536585223407,-4.82344790705798,335.971136013064));
#56941=CARTESIAN_POINT('Ctrl Pts',(103.528689623861,-4.79387191458711,336.10792454456));
#56942=CARTESIAN_POINT('Ctrl Pts',(103.520794024314,-4.75855712104157,336.243107874758));
#56943=CARTESIAN_POINT('Ctrl Pts',(103.512886603557,-4.72318945454764,336.378493600057));
#56944=CARTESIAN_POINT('Ctrl Pts',(103.5049791828,-4.68206591424285,336.512268963163));
#56945=CARTESIAN_POINT('Ctrl Pts',(103.497071762043,-4.63537159557901,336.643932247205));
#56946=CARTESIAN_POINT('Ctrl Pts',(103.489158134885,-4.58864062733358,336.775698871533));
#56947=CARTESIAN_POINT('Ctrl Pts',(103.481244507727,-4.53633030194542,336.905349768461));
#56948=CARTESIAN_POINT('Ctrl Pts',(103.473330880569,-4.47867326865673,337.032404687832));
#56949=CARTESIAN_POINT('Ctrl Pts',(103.465402634855,-4.42090972762745,337.159694311133));
#56950=CARTESIAN_POINT('Ctrl Pts',(103.457474389141,-4.35777990602733,337.284378041659));
#56951=CARTESIAN_POINT('Ctrl Pts',(103.449546143427,-4.28956225889343,337.406000558931));
#56952=CARTESIAN_POINT('Ctrl Pts',(103.442929007605,-4.23262590085788,337.507510116642));
#56953=CARTESIAN_POINT('Ctrl Pts',(103.436311871783,-4.17214620241084,337.606887630587));
#56954=CARTESIAN_POINT('Ctrl Pts',(103.429694735961,-4.10830708304314,337.703885347776));
#56955=CARTESIAN_POINT('Ctrl Pts',(103.421919657183,-4.03329665624005,337.817856847341));
#56956=CARTESIAN_POINT('Ctrl Pts',(103.414144578404,-3.95342145703706,337.928884701484));
#56957=CARTESIAN_POINT('Ctrl Pts',(103.406369499626,-3.86893973295263,338.036525712929));
#56958=CARTESIAN_POINT('Ctrl Pts',(103.398603988577,-3.78456196900823,338.144034265257));
#56959=CARTESIAN_POINT('Ctrl Pts',(103.390838477528,-3.69558919813373,338.248163962923));
#56960=CARTESIAN_POINT('Ctrl Pts',(103.383072966479,-3.60232376947725,338.348499144745));
#56961=CARTESIAN_POINT('Ctrl Pts',(103.375315154957,-3.50915081376474,338.448734843943));
#56962=CARTESIAN_POINT('Ctrl Pts',(103.367557343434,-3.41169393471967,338.545183229985));
#56963=CARTESIAN_POINT('Ctrl Pts',(103.359799531912,-3.31029647385732,338.637460696374));
#56964=CARTESIAN_POINT('Ctrl Pts',(103.352047558389,-3.20897531779949,338.729668721044));
#56965=CARTESIAN_POINT('Ctrl Pts',(103.344295584866,-3.10371977035404,338.817711811562));
#56966=CARTESIAN_POINT('Ctrl Pts',(103.336543611343,-2.99491058842981,338.901242575105));
#56967=CARTESIAN_POINT('Ctrl Pts',(103.328794920785,-2.88614748725895,338.984737963319));
#56968=CARTESIAN_POINT('Ctrl Pts',(103.321046230228,-2.77383405428439,339.063724587826));
#56969=CARTESIAN_POINT('Ctrl Pts',(103.31329753967,-2.65838457234053,339.137894939222));
#56970=CARTESIAN_POINT('Ctrl Pts',(103.305550461292,-2.54295911062556,339.212049858858));
#56971=CARTESIAN_POINT('Ctrl Pts',(103.297803382915,-2.42439922642217,339.281390287423));
#56972=CARTESIAN_POINT('Ctrl Pts',(103.290056304537,-2.30314833251895,339.34565194429));
#56973=CARTESIAN_POINT('Ctrl Pts',(103.282309161231,-2.18189642241679,339.409914139732));
#56974=CARTESIAN_POINT('Ctrl Pts',(103.274562017925,-2.05795380299812,339.469097295537));
#56975=CARTESIAN_POINT('Ctrl Pts',(103.266814874619,-1.93178828353325,339.522983206923));
#56976=CARTESIAN_POINT('Ctrl Pts',(103.259065989591,-1.80559439938113,339.576881233005));
#56977=CARTESIAN_POINT('Ctrl Pts',(103.251317104563,-1.67717698011644,339.625479491349));
#56978=CARTESIAN_POINT('Ctrl Pts',(103.243568219535,-1.54702321632472,339.668608168464));
#56979=CARTESIAN_POINT('Ctrl Pts',(103.23581110976,-1.41673130598302,339.711782622804));
#56980=CARTESIAN_POINT('Ctrl Pts',(103.228053999986,-1.284699741221,339.749475775802));
#56981=CARTESIAN_POINT('Ctrl Pts',(103.220296890211,-1.15143079348762,339.781567754441));
#56982=CARTESIAN_POINT('Ctrl Pts',(103.212535635285,-1.0180906310896,339.813676882007));
#56983=CARTESIAN_POINT('Ctrl Pts',(103.204774380358,-0.883512151498329,
339.840178795731));
#56984=CARTESIAN_POINT('Ctrl Pts',(103.197013125432,-0.74820620472424,339.861005095421));
#56985=CARTESIAN_POINT('Ctrl Pts',(103.189239455028,-0.612683812531602,
339.881864710404));
#56986=CARTESIAN_POINT('Ctrl Pts',(103.181465784623,-0.476432016397678,
339.897030525293));
#56987=CARTESIAN_POINT('Ctrl Pts',(103.173692114218,-0.339966046539224,
339.906486130593));
#56988=CARTESIAN_POINT('Ctrl Pts',(103.166280310041,-0.20985260041005,339.915501575191));
#56989=CARTESIAN_POINT('Ctrl Pts',(103.158868505864,-0.079544759074796,
339.91932645848));
#56990=CARTESIAN_POINT('Ctrl Pts',(103.151456701687,0.0505141765631969,
339.917990583609));
#56991=CARTESIAN_POINT('Ctrl Pts',(103.143681622909,0.186947688063153,339.916589233531));
#56992=CARTESIAN_POINT('Ctrl Pts',(103.13590654413,0.323538432814568,339.909504017112));
#56993=CARTESIAN_POINT('Ctrl Pts',(103.128131465352,0.459773964221454,339.896712260724));
#56994=CARTESIAN_POINT('Ctrl Pts',(103.120365954303,0.595841849133858,339.883936245406));
#56995=CARTESIAN_POINT('Ctrl Pts',(103.112600443254,0.731555004988187,339.865467698595));
#56996=CARTESIAN_POINT('Ctrl Pts',(103.104834932205,0.866400274955407,339.841335934022));
#56997=CARTESIAN_POINT('Ctrl Pts',(103.097077120682,1.00111184544505,339.817228096165));
#56998=CARTESIAN_POINT('Ctrl Pts',(103.08931930916,1.13495686023082,339.787468283319));
#56999=CARTESIAN_POINT('Ctrl Pts',(103.081561497638,1.26742693462888,339.752137627203));
#57000=CARTESIAN_POINT('Ctrl Pts',(103.073809524115,1.39979732109473,339.716833558526));
#57001=CARTESIAN_POINT('Ctrl Pts',(103.066057550592,1.53079445051333,339.675967091341));
#57002=CARTESIAN_POINT('Ctrl Pts',(103.058305577069,1.65992014343549,339.629670418066));
#57003=CARTESIAN_POINT('Ctrl Pts',(103.050556886511,1.78899115155012,339.58339335146));
#57004=CARTESIAN_POINT('Ctrl Pts',(103.042808195954,1.91619193232941,339.531690784341));
#57005=CARTESIAN_POINT('Ctrl Pts',(103.035059505396,2.04103970234368,339.474744685002));
#57006=CARTESIAN_POINT('Ctrl Pts',(103.027312427018,2.16586149673648,339.417810433775));
#57007=CARTESIAN_POINT('Ctrl Pts',(103.01956534864,2.28833089873702,339.355634982434));
#57008=CARTESIAN_POINT('Ctrl Pts',(103.011818270262,2.40798571302497,339.28844818884));
#57009=CARTESIAN_POINT('Ctrl Pts',(103.004071126957,2.52764153013551,339.221260832157));
#57010=CARTESIAN_POINT('Ctrl Pts',(102.996323983651,2.64448237166226,339.149062240822));
#57011=CARTESIAN_POINT('Ctrl Pts',(102.988576840345,2.75807158611075,339.072127722504));
#57012=CARTESIAN_POINT('Ctrl Pts',(102.980827955317,2.87168633782614,338.995175907674));
#57013=CARTESIAN_POINT('Ctrl Pts',(102.973079070289,2.98204768421959,338.913486266305));
#57014=CARTESIAN_POINT('Ctrl Pts',(102.965330185261,3.08874917872546,338.827376591534));
#57015=CARTESIAN_POINT('Ctrl Pts',(102.957573075486,3.19556392730025,338.741175519064));
#57016=CARTESIAN_POINT('Ctrl Pts',(102.949815965711,3.29871075946694,338.650545287406));
#57017=CARTESIAN_POINT('Ctrl Pts',(102.942058855936,3.39781706354589,338.555843397167));
#57018=CARTESIAN_POINT('Ctrl Pts',(102.93429760101,3.49697632686494,338.461090901266));
#57019=CARTESIAN_POINT('Ctrl Pts',(102.926536346084,3.59209048892746,338.362262692867));
#57020=CARTESIAN_POINT('Ctrl Pts',(102.918775091158,3.6828255802995,338.259751341374));
#57021=CARTESIAN_POINT('Ctrl Pts',(102.911001420753,3.77370581824706,338.157076005127));
#57022=CARTESIAN_POINT('Ctrl Pts',(102.903227750349,3.86019274055043,338.050706055605));
#57023=CARTESIAN_POINT('Ctrl Pts',(102.895454079944,3.94199372747953,337.941065880767));
#57024=CARTESIAN_POINT('Ctrl Pts',(102.888042275767,4.01998685878547,337.836529482448));
#57025=CARTESIAN_POINT('Ctrl Pts',(102.88063047159,4.09372033475148,337.729020702494));
#57026=CARTESIAN_POINT('Ctrl Pts',(102.873218667413,4.16297932192538,337.618928450287));
#57027=CARTESIAN_POINT('Ctrl Pts',(102.865443588635,4.23563289837379,337.503440248849));
#57028=CARTESIAN_POINT('Ctrl Pts',(102.857668509856,4.30359187829115,337.384743960398));
#57029=CARTESIAN_POINT('Ctrl Pts',(102.849893431078,4.36655988068137,337.263258242208));
#57030=CARTESIAN_POINT('Ctrl Pts',(102.842127920029,4.42945039693583,337.141922019929));
#57031=CARTESIAN_POINT('Ctrl Pts',(102.83436240898,4.48736197776486,337.017803541454));
#57032=CARTESIAN_POINT('Ctrl Pts',(102.826596897931,4.54004157510634,336.891350194651));
#57033=CARTESIAN_POINT('Ctrl Pts',(102.818839086409,4.59266894047375,336.765022226709));
#57034=CARTESIAN_POINT('Ctrl Pts',(102.811081274886,4.64007449647996,336.63636435597));
#57035=CARTESIAN_POINT('Ctrl Pts',(102.803323463364,4.68205135239322,336.505847998987));
#57036=CARTESIAN_POINT('Ctrl Pts',(102.795571489841,4.72399661939116,336.375429859702));
#57037=CARTESIAN_POINT('Ctrl Pts',(102.787819516318,4.76052119863007,336.243156388562));
#57038=CARTESIAN_POINT('Ctrl Pts',(102.780067542795,4.79146666004779,336.109518052197));
#57039=CARTESIAN_POINT('Ctrl Pts',(102.772318852238,4.82239901604427,335.975936311746));
#57040=CARTESIAN_POINT('Ctrl Pts',(102.76457016168,4.84775686558752,335.840991235719));
#57041=CARTESIAN_POINT('Ctrl Pts',(102.756821471122,4.86743196788014,335.705187280485));
#57042=CARTESIAN_POINT('Ctrl Pts',(102.749074392745,4.88710297660338,335.569411580399));
#57043=CARTESIAN_POINT('Ctrl Pts',(102.741327314367,4.90109353383086,335.43277774314));
#57044=CARTESIAN_POINT('Ctrl Pts',(102.733580235989,4.90934681153394,335.295798827891));
#57045=CARTESIAN_POINT('Ctrl Pts',(102.725833092683,4.91760015840744,335.158818764627));
#57046=CARTESIAN_POINT('Ctrl Pts',(102.718085949377,4.92011610634116,335.021494007772));
#57047=CARTESIAN_POINT('Ctrl Pts',(102.710338806072,4.91688987024794,334.884340731659));
#57048=CARTESIAN_POINT('Ctrl Pts',(102.702589921043,4.91366290882836,334.747156620578));
#57049=CARTESIAN_POINT('Ctrl Pts',(102.694841036015,4.90469120369609,334.610144457645));
#57050=CARTESIAN_POINT('Ctrl Pts',(102.687092150987,4.89002204231956,334.473818008548));
#57051=CARTESIAN_POINT('Ctrl Pts',(102.679335041213,4.87533731094359,334.337346861149));
#57052=CARTESIAN_POINT('Ctrl Pts',(102.671577931438,4.85494308508052,334.201563270727));
#57053=CARTESIAN_POINT('Ctrl Pts',(102.663820821663,4.82893835305869,334.066974038486));
#57054=CARTESIAN_POINT('Ctrl Pts',(102.656059566737,4.80291972493951,333.932312886062));
#57055=CARTESIAN_POINT('Ctrl Pts',(102.648298311811,4.77128470683159,333.798847743687));
#57056=CARTESIAN_POINT('Ctrl Pts',(102.640537056885,4.73418268869762,333.667071895211));
#57057=CARTESIAN_POINT('Ctrl Pts',(102.63276338648,4.69702131942618,333.535085248324));
#57058=CARTESIAN_POINT('Ctrl Pts',(102.624989716076,4.65437559584653,333.404793667048));
#57059=CARTESIAN_POINT('Ctrl Pts',(102.617216045671,4.60644404152253,333.276672882236));
#57060=CARTESIAN_POINT('Ctrl Pts',(102.609804241494,4.56074371258291,333.154516150778));
#57061=CARTESIAN_POINT('Ctrl Pts',(102.602392437316,4.51023870059003,333.034332928113));
#57062=CARTESIAN_POINT('Ctrl Pts',(102.594980633139,4.455139789031,332.916514333456));
#57063=CARTESIAN_POINT('Ctrl Pts',(102.587205554361,4.39734031568635,332.792921098515));
#57064=CARTESIAN_POINT('Ctrl Pts',(102.579430475582,4.33430257797251,332.671539569988));
#57065=CARTESIAN_POINT('Ctrl Pts',(102.571655396804,4.26621824495883,332.552845540453));
#57066=CARTESIAN_POINT('Ctrl Pts',(102.563889885755,4.19821769405148,332.434297571478));
#57067=CARTESIAN_POINT('Ctrl Pts',(102.556124374706,4.12518309690227,332.318430857049));
#57068=CARTESIAN_POINT('Ctrl Pts',(102.548358863657,4.04735373268759,332.205700297928));
#57069=CARTESIAN_POINT('Ctrl Pts',(102.540601052135,3.96960153651417,332.093081511484));
#57070=CARTESIAN_POINT('Ctrl Pts',(102.532843240613,3.88706425469921,331.983593011841));
#57071=CARTESIAN_POINT('Ctrl Pts',(102.52508542909,3.80002635103384,331.877663888376));
#57072=CARTESIAN_POINT('Ctrl Pts',(102.517333455567,3.71305394615075,331.771814479936));
#57073=CARTESIAN_POINT('Ctrl Pts',(102.509581482044,3.62158790794401,331.669519416952));
#57074=CARTESIAN_POINT('Ctrl Pts',(102.501829508521,3.52595494466814,331.571177346279));
#57075=CARTESIAN_POINT('Ctrl Pts',(102.494080817964,3.43036248200924,331.472876923532));
#57076=CARTESIAN_POINT('Ctrl Pts',(102.486332127406,3.33060687607175,331.37852644308));
#57077=CARTESIAN_POINT('Ctrl Pts',(102.478583436848,3.22705375967267,331.288489917206));
#57078=CARTESIAN_POINT('Ctrl Pts',(102.470836358471,3.12352218836428,331.198472124183));
#57079=CARTESIAN_POINT('Ctrl Pts',(102.463089280093,3.0161949729509,331.112766756746));
#57080=CARTESIAN_POINT('Ctrl Pts',(102.455342201715,2.90547280293872,331.031699248559));
#57081=CARTESIAN_POINT('Ctrl Pts',(102.447595058409,2.79474970496796,330.950631060949));
#57082=CARTESIAN_POINT('Ctrl Pts',(102.439847915103,2.68063191102454,330.874201041029));
#57083=CARTESIAN_POINT('Ctrl Pts',(102.432100771797,2.5635508936325,330.802692544231));
#57084=CARTESIAN_POINT('Ctrl Pts',(102.424351886769,2.44644355394213,330.731167970804));
#57085=CARTESIAN_POINT('Ctrl Pts',(102.416603001741,2.32637199866117,330.664567325933));
#57086=CARTESIAN_POINT('Ctrl Pts',(102.408854116713,2.20379385428027,330.603128872671));
#57087=CARTESIAN_POINT('Ctrl Pts',(102.401097006938,2.0810856041907,330.541625208));
#57088=CARTESIAN_POINT('Ctrl Pts',(102.393339897164,1.95586580035378,330.485294855583));
#57089=CARTESIAN_POINT('Ctrl Pts',(102.385582787389,1.82861419097799,330.434328833232));
#57090=CARTESIAN_POINT('Ctrl Pts',(102.377821532463,1.70129458241061,330.383335576269));
#57091=CARTESIAN_POINT('Ctrl Pts',(102.370060277537,1.57194137331711,330.337712491132));
#57092=CARTESIAN_POINT('Ctrl Pts',(102.36229902261,1.44105022009306,330.297600896811));
#57093=CARTESIAN_POINT('Ctrl Pts',(102.354525352206,1.30994968368136,330.257425137012));
#57094=CARTESIAN_POINT('Ctrl Pts',(102.346751681801,1.17730666529713,330.22277858502));
#57095=CARTESIAN_POINT('Ctrl Pts',(102.338978011396,1.04362864965377,330.193751743395));
#57096=CARTESIAN_POINT('Ctrl Pts',(102.331566207219,0.916173377803752,330.166076108232));
#57097=CARTESIAN_POINT('Ctrl Pts',(102.324154403043,0.787777581908544,330.143508812399));
#57098=CARTESIAN_POINT('Ctrl Pts',(102.316742598866,0.658884229499549,330.126084260616));
#57099=CARTESIAN_POINT('Ctrl Pts',(102.308967520087,0.523673429931368,330.107805679644));
#57100=CARTESIAN_POINT('Ctrl Pts',(102.301192441309,0.387487776050841,330.095128948182));
#57101=CARTESIAN_POINT('Ctrl Pts',(102.29341736253,0.250831095116849,330.088150366285));
#57102=CARTESIAN_POINT('Ctrl Pts',(102.285651851481,0.114342578928736,330.081180371978));
#57103=CARTESIAN_POINT('Ctrl Pts',(102.277886340432,-0.0226154243838896,
330.079894595237));
#57104=CARTESIAN_POINT('Ctrl Pts',(102.270120829383,-0.159530891374533,
330.084337994004));
#57105=CARTESIAN_POINT('Ctrl Pts',(102.262363017861,-0.29631060628113,330.088776987127));
#57106=CARTESIAN_POINT('Ctrl Pts',(102.254605206339,-0.43304748064413,330.098933838655));
#57107=CARTESIAN_POINT('Ctrl Pts',(102.246847394817,-0.569226744371924,
330.114801541801));
#57108=CARTESIAN_POINT('Ctrl Pts',(102.239095421294,-0.705303528885548,
330.130657303997));
#57109=CARTESIAN_POINT('Ctrl Pts',(102.231343447771,-0.840823151312165,
330.152215318597));
#57110=CARTESIAN_POINT('Ctrl Pts',(102.223591474248,-0.975273580423576,
330.179416580348));
#57111=CARTESIAN_POINT('Ctrl Pts',(102.21584278369,-1.10966706969789,330.206606322348));
#57112=CARTESIAN_POINT('Ctrl Pts',(102.208094093132,-1.24299188393726,330.239434480771));
#57113=CARTESIAN_POINT('Ctrl Pts',(102.200345402575,-1.37474405254973,330.277790575114));
#57114=CARTESIAN_POINT('Ctrl Pts',(102.192598324197,-1.506468809023,330.316138689152));
#57115=CARTESIAN_POINT('Ctrl Pts',(102.184851245819,-1.63662119563893,330.360012342225));
#57116=CARTESIAN_POINT('Ctrl Pts',(102.177104167441,-1.76471071220216,330.40925069681));
#57117=CARTESIAN_POINT('Ctrl Pts',(102.169357024135,-1.89280130227917,330.45848946406));
#57118=CARTESIAN_POINT('Ctrl Pts',(102.161609880829,-2.01882862297318,330.51309288225));
#57119=CARTESIAN_POINT('Ctrl Pts',(102.153862737524,-2.14232090011578,330.572851456815));
#57120=CARTESIAN_POINT('Ctrl Pts',(102.146113852495,-2.26584094094325,330.632623466375));
#57121=CARTESIAN_POINT('Ctrl Pts',(102.138364967467,-2.3868244523435,330.697552768341));
#57122=CARTESIAN_POINT('Ctrl Pts',(102.130616082439,-2.50482342587954,330.767383472642));
#57123=CARTESIAN_POINT('Ctrl Pts',(102.122858972665,-2.6229476447459,330.837288295975));
#57124=CARTESIAN_POINT('Ctrl Pts',(102.11510186289,-2.73808066081635,330.91210471454));
#57125=CARTESIAN_POINT('Ctrl Pts',(102.107344753115,-2.84980222385214,330.991532668534));
#57126=CARTESIAN_POINT('Ctrl Pts',(102.099583498189,-2.96158348731882,331.071003066288));
#57127=CARTESIAN_POINT('Ctrl Pts',(102.091822243263,-3.06994935666206,331.155089670224));
#57128=CARTESIAN_POINT('Ctrl Pts',(102.084060988337,-3.17451276561177,331.24345214812));
#57129=CARTESIAN_POINT('Ctrl Pts',(102.076287317932,-3.27924344193879,331.331955977183));
#57130=CARTESIAN_POINT('Ctrl Pts',(102.068513647527,-3.38015921496347,331.424749083855));
#57131=CARTESIAN_POINT('Ctrl Pts',(102.060739977123,-3.47690935005386,331.521453689541));
#57132=CARTESIAN_POINT('Ctrl Pts',(102.053328172945,-3.56915574308011,331.613656672568));
#57133=CARTESIAN_POINT('Ctrl Pts',(102.045916368768,-3.6576153961095,331.709414977858));
#57134=CARTESIAN_POINT('Ctrl Pts',(102.038504564591,-3.74201966233167,331.808374722931));
#57135=CARTESIAN_POINT('Ctrl Pts',(102.03078102222,-3.8299739459106,331.911496684304));
#57136=CARTESIAN_POINT('Ctrl Pts',(102.02305747985,-3.91381268601028,332.018433581657));
#57137=CARTESIAN_POINT('Ctrl Pts',(102.015333937479,-3.99318321602257,332.128820648971));
#57138=CARTESIAN_POINT('Ctrl Pts',(102.007622832742,-4.07242593142545,332.239029954086));
#57139=CARTESIAN_POINT('Ctrl Pts',(101.999911728005,-4.14721453531853,332.352678046835));
#57140=CARTESIAN_POINT('Ctrl Pts',(101.992200623267,-4.21723515906342,332.469365558667));
#57141=CARTESIAN_POINT('Ctrl Pts',(101.984496712,-4.28719046256242,332.585944216043));
#57142=CARTESIAN_POINT('Ctrl Pts',(101.976792800733,-4.35238642900278,332.705556316164));
#57143=CARTESIAN_POINT('Ctrl Pts',(101.969088889465,-4.41255109860553,332.82777168219));
#57144=CARTESIAN_POINT('Ctrl Pts',(101.961390440342,-4.47267311090889,332.949900396407));
#57145=CARTESIAN_POINT('Ctrl Pts',(101.953691991218,-4.52777074797215,333.074628350676));
#57146=CARTESIAN_POINT('Ctrl Pts',(101.945993542094,-4.57761706477003,333.201499215784));
#57147=CARTESIAN_POINT('Ctrl Pts',(101.93829882817,-4.62743919670017,333.328308524586));
#57148=CARTESIAN_POINT('Ctrl Pts',(101.930604114246,-4.67201493381984,333.457258306925));
#57149=CARTESIAN_POINT('Ctrl Pts',(101.922909400323,-4.71116491965499,333.587871053228));
#57150=CARTESIAN_POINT('Ctrl Pts',(101.915215346244,-4.75031154826039,333.718472599092));
#57151=CARTESIAN_POINT('Ctrl Pts',(101.907521292165,-4.78403322919711,333.850736448018));
#57152=CARTESIAN_POINT('Ctrl Pts',(101.899827238087,-4.81220014008847,333.984168875141));
#57153=CARTESIAN_POINT('Ctrl Pts',(101.892133632618,-4.84036540867839,334.117593522346));
#57154=CARTESIAN_POINT('Ctrl Pts',(101.884440027149,-4.86297647519989,334.252186222965));
#57155=CARTESIAN_POINT('Ctrl Pts',(101.876746421681,-4.8799545760377,334.387442738751));
#57156=CARTESIAN_POINT('Ctrl Pts',(101.869049202525,-4.89694065148953,334.522762784523));
#57157=CARTESIAN_POINT('Ctrl Pts',(101.86135198337,-4.90828843265978,334.658746873884));
#57158=CARTESIAN_POINT('Ctrl Pts',(101.853654764215,-4.91397100480007,334.794885333328));
#57159=CARTESIAN_POINT('Ctrl Pts',(101.849708968313,-4.91688403993803,334.864673469087));
#57160=CARTESIAN_POINT('Ctrl Pts',(101.845763172411,-4.91830918249373,334.934502131675));
#57161=CARTESIAN_POINT('Ctrl Pts',(101.841817376509,-4.91824811790597,335.004302698495));
#57162=CARTESIAN_POINT('',(100.091817376546,-4.91824999882167,335.00010765993));
#57163=CARTESIAN_POINT('Ctrl Pts',(101.841817376472,-4.91824811790539,335.004302699159));
#57164=CARTESIAN_POINT('Ctrl Pts',(101.832410613969,-4.91810254013675,335.17070698639));
#57165=CARTESIAN_POINT('Ctrl Pts',(101.823003851466,-4.90950805915332,335.33674024558));
#57166=CARTESIAN_POINT('Ctrl Pts',(101.813597088963,-4.8925997979356,335.501647565269));
#57167=CARTESIAN_POINT('Ctrl Pts',(101.804058433833,-4.87545446525098,335.66886705767));
#57168=CARTESIAN_POINT('Ctrl Pts',(101.794519778704,-4.84976063729519,335.834928835721));
#57169=CARTESIAN_POINT('Ctrl Pts',(101.784981123574,-4.81570820956695,335.999068317388));
#57170=CARTESIAN_POINT('Ctrl Pts',(101.776742925822,-4.78629833681709,336.140829759703));
#57171=CARTESIAN_POINT('Ctrl Pts',(101.76850472807,-4.75065445968432,336.281157717628));
#57172=CARTESIAN_POINT('Ctrl Pts',(101.760266530318,-4.70892734215704,336.419572593701));
#57173=CARTESIAN_POINT('Ctrl Pts',(101.752491451539,-4.66954595854219,336.550206331559));
#57174=CARTESIAN_POINT('Ctrl Pts',(101.744716372761,-4.62466221922097,336.679406493277));
#57175=CARTESIAN_POINT('Ctrl Pts',(101.736941293982,-4.57439721182412,336.806674627861));
#57176=CARTESIAN_POINT('Ctrl Pts',(101.729175782933,-4.52419405871887,336.933786150903));
#57177=CARTESIAN_POINT('Ctrl Pts',(101.721410271884,-4.46862295561675,337.058970017249));
#57178=CARTESIAN_POINT('Ctrl Pts',(101.713644760835,-4.40785511440055,337.181741587116));
#57179=CARTESIAN_POINT('Ctrl Pts',(101.705886949313,-4.34714752467597,337.304391428615));
#57180=CARTESIAN_POINT('Ctrl Pts',(101.698129137791,-4.28125362304016,337.424633385396));
#57181=CARTESIAN_POINT('Ctrl Pts',(101.690371326269,-4.21039305456203,337.542001846694));
#57182=CARTESIAN_POINT('Ctrl Pts',(101.682619352746,-4.13958581090865,337.659281984503));
#57183=CARTESIAN_POINT('Ctrl Pts',(101.674867379223,-4.06381954108214,337.773692597702));
#57184=CARTESIAN_POINT('Ctrl Pts',(101.6671154057,-3.98336008141318,337.884792111107));
#57185=CARTESIAN_POINT('Ctrl Pts',(101.659366715142,-3.90293469637327,337.995844573801));
#57186=CARTESIAN_POINT('Ctrl Pts',(101.651618024585,-3.81782030341457,338.103588409767));
#57187=CARTESIAN_POINT('Ctrl Pts',(101.643869334027,-3.72832624913155,338.207610706201));
#57188=CARTESIAN_POINT('Ctrl Pts',(101.636122255649,-3.63885081483393,338.311611359927));
#57189=CARTESIAN_POINT('Ctrl Pts',(101.628375177271,-3.54499778646565,338.411891718134));
#57190=CARTESIAN_POINT('Ctrl Pts',(101.620628098893,-3.44711676188987,338.508071990766));
#57191=CARTESIAN_POINT('Ctrl Pts',(101.612880955588,-3.34923491697709,338.604253069482));
#57192=CARTESIAN_POINT('Ctrl Pts',(101.605133812282,-3.24732528732444,338.696333720127));
#57193=CARTESIAN_POINT('Ctrl Pts',(101.597386668976,-3.14177399744879,338.783971354471));
#57194=CARTESIAN_POINT('Ctrl Pts',(101.589637783948,-3.03619897740227,338.871628691615));
#57195=CARTESIAN_POINT('Ctrl Pts',(101.58188889892,-2.92698096863593,338.954840775147));
#57196=CARTESIAN_POINT('Ctrl Pts',(101.574140013892,-2.81453847606166,339.033305868549));
#57197=CARTESIAN_POINT('Ctrl Pts',(101.566382904117,-2.70197663586379,339.111854245612));
#57198=CARTESIAN_POINT('Ctrl Pts',(101.558625794342,-2.58618379614258,339.185645343623));
#57199=CARTESIAN_POINT('Ctrl Pts',(101.550868684568,-2.46760716237224,339.25442098936));
#57200=CARTESIAN_POINT('Ctrl Pts',(101.543107429642,-2.34896716504017,339.323233386604));
#57201=CARTESIAN_POINT('Ctrl Pts',(101.535346174715,-2.22754075539452,339.387024809543));
#57202=CARTESIAN_POINT('Ctrl Pts',(101.527584919789,-2.10379804448129,339.445583971824));
#57203=CARTESIAN_POINT('Ctrl Pts',(101.519811249385,-1.97985738555834,339.50423680968));
#57204=CARTESIAN_POINT('Ctrl Pts',(101.51203757898,-1.8535933812147,339.557640508971));
#57205=CARTESIAN_POINT('Ctrl Pts',(101.504263908575,-1.7254951718925,339.605632364212));
#57206=CARTESIAN_POINT('Ctrl Pts',(101.496852104398,-1.60335996503264,339.651390187045));
#57207=CARTESIAN_POINT('Ctrl Pts',(101.489440300221,-1.4795577480398,339.692228579685));
#57208=CARTESIAN_POINT('Ctrl Pts',(101.482028496044,-1.35452190374054,339.728049648088));
#57209=CARTESIAN_POINT('Ctrl Pts',(101.474253417266,-1.2233576802498,339.765626413759));
#57210=CARTESIAN_POINT('Ctrl Pts',(101.466478338487,-1.09042134112152,339.79780034082));
#57211=CARTESIAN_POINT('Ctrl Pts',(101.458703259709,-0.9561975718951,339.824403514011));
#57212=CARTESIAN_POINT('Ctrl Pts',(101.45093774866,-0.822138973561904,339.850973950303));
#57213=CARTESIAN_POINT('Ctrl Pts',(101.443172237611,-0.686796477113662,
339.871987197276));
#57214=CARTESIAN_POINT('Ctrl Pts',(101.435406726562,-0.550670279055428,
339.887324964259));
#57215=CARTESIAN_POINT('Ctrl Pts',(101.427648915039,-0.41467905051889,339.902647523801));
#57216=CARTESIAN_POINT('Ctrl Pts',(101.419891103517,-0.277906052645194,
339.912305758427));
#57217=CARTESIAN_POINT('Ctrl Pts',(101.412133291995,-0.140861690011362,
339.916232403659));
#57218=CARTESIAN_POINT('Ctrl Pts',(101.404381318472,-0.00392045760633933,
339.920156093966));
#57219=CARTESIAN_POINT('Ctrl Pts',(101.396629344949,0.133291343946892,339.918356768948));
#57220=CARTESIAN_POINT('Ctrl Pts',(101.388877371426,0.270258525362551,339.910819014377));
#57221=CARTESIAN_POINT('Ctrl Pts',(101.381128680868,0.407167701095562,339.90328445205));
#57222=CARTESIAN_POINT('Ctrl Pts',(101.373379990311,0.543832073266215,339.890016315156));
#57223=CARTESIAN_POINT('Ctrl Pts',(101.365631299753,0.679737009496073,339.871051289036));
#57224=CARTESIAN_POINT('Ctrl Pts',(101.357884221375,0.815613669568848,339.852090208748));
#57225=CARTESIAN_POINT('Ctrl Pts',(101.350137142998,0.950730821107749,339.827434650838));
#57226=CARTESIAN_POINT('Ctrl Pts',(101.34239006462,1.08457990309042,339.797173073417));
#57227=CARTESIAN_POINT('Ctrl Pts',(101.334642921314,1.21843010685722,339.766911242374));
#57228=CARTESIAN_POINT('Ctrl Pts',(101.326895778008,1.35101183861837,339.731043384303));
#57229=CARTESIAN_POINT('Ctrl Pts',(101.319148634702,1.48182805448822,339.689708805398));
#57230=CARTESIAN_POINT('Ctrl Pts',(101.311399749674,1.61267368062071,339.648364933603));
#57231=CARTESIAN_POINT('Ctrl Pts',(101.303650864646,1.74175262838628,339.601552013074));
#57232=CARTESIAN_POINT('Ctrl Pts',(101.295901979618,1.86858468408841,339.549458686579));
#57233=CARTESIAN_POINT('Ctrl Pts',(101.288144869843,1.99555136064496,339.497310067689));
#57234=CARTESIAN_POINT('Ctrl Pts',(101.280387760069,2.12026601899166,339.439869995702));
#57235=CARTESIAN_POINT('Ctrl Pts',(101.272630650294,2.2422695472152,339.377374822897));
#57236=CARTESIAN_POINT('Ctrl Pts',(101.264869395368,2.36433827022323,339.31484625467));
#57237=CARTESIAN_POINT('Ctrl Pts',(101.257108140441,2.48369263640856,339.247257395584));
#57238=CARTESIAN_POINT('Ctrl Pts',(101.249346885515,2.59990056650561,339.174889232876));
#57239=CARTESIAN_POINT('Ctrl Pts',(101.241573215111,2.71629439141875,339.102405304693));
#57240=CARTESIAN_POINT('Ctrl Pts',(101.233799544706,2.82953139924868,339.025127015706));
#57241=CARTESIAN_POINT('Ctrl Pts',(101.226025874301,2.9392100655196,338.943377645274));
#57242=CARTESIAN_POINT('Ctrl Pts',(101.218614070124,3.04378316348874,338.865433727703));
#57243=CARTESIAN_POINT('Ctrl Pts',(101.211202265947,3.14512152249386,338.783425799794));
#57244=CARTESIAN_POINT('Ctrl Pts',(101.20379046177,3.24290829302842,338.697665326325));
#57245=CARTESIAN_POINT('Ctrl Pts',(101.196015382992,3.34548788447835,338.607701476585));
#57246=CARTESIAN_POINT('Ctrl Pts',(101.188240304213,3.4444831071328,338.513323631012));
#57247=CARTESIAN_POINT('Ctrl Pts',(101.180465225435,3.53949046630928,338.414848503434));
#57248=CARTESIAN_POINT('Ctrl Pts',(101.172699714386,3.63438091288183,338.31649455577));
#57249=CARTESIAN_POINT('Ctrl Pts',(101.164934203337,3.72529299133774,338.214053636778));
#57250=CARTESIAN_POINT('Ctrl Pts',(101.157168692288,3.81185654349949,338.107882358501));
#57251=CARTESIAN_POINT('Ctrl Pts',(101.149410880766,3.8983342676472,338.001816349355));
#57252=CARTESIAN_POINT('Ctrl Pts',(101.141653069243,3.98047180037617,337.892027642465));
#57253=CARTESIAN_POINT('Ctrl Pts',(101.133895257721,4.05793636834805,337.778909047259));
#57254=CARTESIAN_POINT('Ctrl Pts',(101.126143284198,4.13534264177599,337.665875577383));
#57255=CARTESIAN_POINT('Ctrl Pts',(101.118391310675,4.2080827300135,337.549517528159));
#57256=CARTESIAN_POINT('Ctrl Pts',(101.110639337152,4.2758648724231,337.430259791726));
#57257=CARTESIAN_POINT('Ctrl Pts',(101.102890646594,4.34361830905519,337.311052561014));
#57258=CARTESIAN_POINT('Ctrl Pts',(101.095141956037,4.40641778325965,337.188948424651));
#57259=CARTESIAN_POINT('Ctrl Pts',(101.087393265479,4.46401564741182,337.064400000524));
#57260=CARTESIAN_POINT('Ctrl Pts',(101.079646187101,4.52160152784723,336.939877489737));
#57261=CARTESIAN_POINT('Ctrl Pts',(101.071899108724,4.57398778691545,336.812912057289));
#57262=CARTESIAN_POINT('Ctrl Pts',(101.064152030346,4.6209735993788,336.683979232753));
#57263=CARTESIAN_POINT('Ctrl Pts',(101.05640488704,4.6679598056285,336.555045327636));
#57264=CARTESIAN_POINT('Ctrl Pts',(101.048657743734,4.70954534116398,336.424144364792));
#57265=CARTESIAN_POINT('Ctrl Pts',(101.040910600428,4.74557837256834,336.291769705602));
#57266=CARTESIAN_POINT('Ctrl Pts',(101.0331617154,4.78161950496313,336.159365285779));
#57267=CARTESIAN_POINT('Ctrl Pts',(101.025412830372,4.81210554656546,336.025486887402));
#57268=CARTESIAN_POINT('Ctrl Pts',(101.017663945344,4.83693525991552,335.890640417838));
#57269=CARTESIAN_POINT('Ctrl Pts',(101.009906835569,4.86179132777987,335.755650820837));
#57270=CARTESIAN_POINT('Ctrl Pts',(101.002149725795,4.88097900357264,335.6196914851));
#57271=CARTESIAN_POINT('Ctrl Pts',(100.99439261602,4.89444858916778,335.483276391409));
#57272=CARTESIAN_POINT('Ctrl Pts',(100.986631361094,4.90792537247879,335.346788401854));
#57273=CARTESIAN_POINT('Ctrl Pts',(100.978870106168,4.91567795502317,335.209844559115));
#57274=CARTESIAN_POINT('Ctrl Pts',(100.971108851241,4.91770880208033,335.072960266184));
#57275=CARTESIAN_POINT('Ctrl Pts',(100.963335180837,4.91974289783093,334.935857002994));
#57276=CARTESIAN_POINT('Ctrl Pts',(100.955561510432,4.91603697843713,334.798813870906));
#57277=CARTESIAN_POINT('Ctrl Pts',(100.947787840027,4.90664560847443,334.662343465429));
#57278=CARTESIAN_POINT('Ctrl Pts',(100.94037603585,4.89769140904286,334.532225790158));
#57279=CARTESIAN_POINT('Ctrl Pts',(100.932964231673,4.88356919375284,334.402629006706));
#57280=CARTESIAN_POINT('Ctrl Pts',(100.925552427496,4.86436941453331,334.273988112044));
#57281=CARTESIAN_POINT('Ctrl Pts',(100.917777348718,4.84422859694115,334.139042143935));
#57282=CARTESIAN_POINT('Ctrl Pts',(100.910002269939,4.81843624845891,334.004721681595));
#57283=CARTESIAN_POINT('Ctrl Pts',(100.902227191161,4.78704034637554,333.871537424337));
#57284=CARTESIAN_POINT('Ctrl Pts',(100.894461680112,4.75568307894844,333.738517058785));
#57285=CARTESIAN_POINT('Ctrl Pts',(100.886696169063,4.71873606687302,333.606630493162));
#57286=CARTESIAN_POINT('Ctrl Pts',(100.878930658014,4.6762988789953,333.476381984614));
#57287=CARTESIAN_POINT('Ctrl Pts',(100.871172846491,4.63390376771292,333.346262617842));
#57288=CARTESIAN_POINT('Ctrl Pts',(100.863415034969,4.58602943385974,333.21777844527));
#57289=CARTESIAN_POINT('Ctrl Pts',(100.855657223447,4.53282611651697,333.091421874818));
#57290=CARTESIAN_POINT('Ctrl Pts',(100.847905249924,4.47966283635768,332.965160391693));
#57291=CARTESIAN_POINT('Ctrl Pts',(100.840153276401,4.42117870594579,332.841023682594));
#57292=CARTESIAN_POINT('Ctrl Pts',(100.832401302878,4.35757313772273,332.719487028781));
#57293=CARTESIAN_POINT('Ctrl Pts',(100.82465261232,4.29399450649563,332.598001845814));
#57294=CARTESIAN_POINT('Ctrl Pts',(100.816903921763,4.2252989321751,332.479114873667));
#57295=CARTESIAN_POINT('Ctrl Pts',(100.809155231205,4.15173301446012,332.363279302023));
#57296=CARTESIAN_POINT('Ctrl Pts',(100.801408152827,4.0781824027487,332.247467830937));
#57297=CARTESIAN_POINT('Ctrl Pts',(100.793661074449,3.99976367261914,332.134706827302));
#57298=CARTESIAN_POINT('Ctrl Pts',(100.785913996072,3.91676802897488,332.025422505683));
#57299=CARTESIAN_POINT('Ctrl Pts',(100.778166852766,3.8337716897473,331.916137268156));
#57300=CARTESIAN_POINT('Ctrl Pts',(100.77041970946,3.7461985968976,331.810329082045));
#57301=CARTESIAN_POINT('Ctrl Pts',(100.762672566154,3.65438146276325,331.708392613462));
#57302=CARTESIAN_POINT('Ctrl Pts',(100.754923681126,3.56254368618781,331.606433227397));
#57303=CARTESIAN_POINT('Ctrl Pts',(100.747174796098,3.4664602312216,331.508347581319));
#57304=CARTESIAN_POINT('Ctrl Pts',(100.73942591107,3.36650174076411,331.414494583475));
#57305=CARTESIAN_POINT('Ctrl Pts',(100.731668801295,3.26643715333202,331.320541969088));
#57306=CARTESIAN_POINT('Ctrl Pts',(100.72391169152,3.16248959970536,331.230831245251));
#57307=CARTESIAN_POINT('Ctrl Pts',(100.716154581746,3.05506440278209,331.14568234867));
#57308=CARTESIAN_POINT('Ctrl Pts',(100.70839332682,2.94758180126844,331.060487951242));
#57309=CARTESIAN_POINT('Ctrl Pts',(100.700632071893,2.83661816959872,330.979860468044));
#57310=CARTESIAN_POINT('Ctrl Pts',(100.692870816967,2.72260825524676,330.904076740103));
#57311=CARTESIAN_POINT('Ctrl Pts',(100.685097146563,2.60841596218758,330.828171782896));
#57312=CARTESIAN_POINT('Ctrl Pts',(100.677323476158,2.49116798309834,330.75712626727));
#57313=CARTESIAN_POINT('Ctrl Pts',(100.669549805753,2.37132489850027,330.691171703554));
#57314=CARTESIAN_POINT('Ctrl Pts',(100.662138001576,2.2570605383238,330.628287340647));
#57315=CARTESIAN_POINT('Ctrl Pts',(100.654726197399,2.14043749726805,330.570030756982));
#57316=CARTESIAN_POINT('Ctrl Pts',(100.647314393222,2.02187052229731,330.516561291423));
#57317=CARTESIAN_POINT('Ctrl Pts',(100.639539314444,1.89749222668933,330.46047112808));
#57318=CARTESIAN_POINT('Ctrl Pts',(100.631764235665,1.77058156457802,330.409471954696));
#57319=CARTESIAN_POINT('Ctrl Pts',(100.623989156887,1.64159395717388,330.363799794846));
#57320=CARTESIAN_POINT('Ctrl Pts',(100.616223645838,1.51276507723248,330.318183837497));
#57321=CARTESIAN_POINT('Ctrl Pts',(100.608458134789,1.38186470227037,330.277881979872));
#57322=CARTESIAN_POINT('Ctrl Pts',(100.60069262374,1.24937075529673,330.243083374884));
#57323=CARTESIAN_POINT('Ctrl Pts',(100.592934812218,1.11700817645717,330.208319272813));
#57324=CARTESIAN_POINT('Ctrl Pts',(100.585177000696,0.983055545574793,330.179047663305));
#57325=CARTESIAN_POINT('Ctrl Pts',(100.577419189173,0.848008241963068,330.155408677291));
#57326=CARTESIAN_POINT('Ctrl Pts',(100.56966721565,0.713062565729998,330.131787480365));
#57327=CARTESIAN_POINT('Ctrl Pts',(100.561915242127,0.57702423992336,330.113790537076));
#57328=CARTESIAN_POINT('Ctrl Pts',(100.554163268604,0.440400852209341,330.10150735921));
#57329=CARTESIAN_POINT('Ctrl Pts',(100.546414578047,0.303835324581131,330.089229383277));
#57330=CARTESIAN_POINT('Ctrl Pts',(100.538665887489,0.166685616344576,330.082660394918));
#57331=CARTESIAN_POINT('Ctrl Pts',(100.530917196931,0.0294662736183612,
330.081838270124));
#57332=CARTESIAN_POINT('Ctrl Pts',(100.523170118554,-0.107724519477521,
330.08101631638));
#57333=CARTESIAN_POINT('Ctrl Pts',(100.515423040176,-0.244984527623456,
330.085938850244));
#57334=CARTESIAN_POINT('Ctrl Pts',(100.507675961798,-0.381797750216591,
330.096591640458));
#57335=CARTESIAN_POINT('Ctrl Pts',(100.499928818492,-0.518612119436214,
330.107244519952));
#57336=CARTESIAN_POINT('Ctrl Pts',(100.492181675186,-0.654979305939604,
330.123627721242));
#57337=CARTESIAN_POINT('Ctrl Pts',(100.484434531881,-0.79038737683619,330.145675035905));
#57338=CARTESIAN_POINT('Ctrl Pts',(100.476685646852,-0.925825890341909,
330.167727307272));
#57339=CARTESIAN_POINT('Ctrl Pts',(100.468936761824,-1.0603044734436,330.195446163158));
#57340=CARTESIAN_POINT('Ctrl Pts',(100.461187876796,-1.19332073640064,330.228714147887));
#57341=CARTESIAN_POINT('Ctrl Pts',(100.453430767022,-1.3264781841935,330.262017443598));
#57342=CARTESIAN_POINT('Ctrl Pts',(100.445673657247,-1.45816983153963,330.300881538798));
#57343=CARTESIAN_POINT('Ctrl Pts',(100.437916547472,-1.58790729335798,330.345138724924));
#57344=CARTESIAN_POINT('Ctrl Pts',(100.430155292546,-1.71771408272773,330.389419560676));
#57345=CARTESIAN_POINT('Ctrl Pts',(100.42239403762,-1.8455642416487,330.43909908829));
#57346=CARTESIAN_POINT('Ctrl Pts',(100.414632782694,-1.97098970179248,330.493961533905));
#57347=CARTESIAN_POINT('Ctrl Pts',(100.406859112289,-2.09661580179643,330.548911741553));
#57348=CARTESIAN_POINT('Ctrl Pts',(100.399085441884,-2.21980910074816,330.60906126345));
#57349=CARTESIAN_POINT('Ctrl Pts',(100.39131177148,-2.34012567012689,330.674148071129));
#57350=CARTESIAN_POINT('Ctrl Pts',(100.383899967302,-2.45484147425528,330.736205072253));
#57351=CARTESIAN_POINT('Ctrl Pts',(100.376488163125,-2.56694209765501,330.802749895338));
#57352=CARTESIAN_POINT('Ctrl Pts',(100.369076358948,-2.6760691054939,330.873519998216));
#57353=CARTESIAN_POINT('Ctrl Pts',(100.361306196586,-2.79047236666394,330.947711811251));
#57354=CARTESIAN_POINT('Ctrl Pts',(100.353536034224,-2.90196984830229,331.026782815924));
#57355=CARTESIAN_POINT('Ctrl Pts',(100.345765871861,-3.01011694758207,331.110478303907));
#57356=CARTESIAN_POINT('Ctrl Pts',(100.338005274769,-3.1181309149972,331.194070760588));
#57357=CARTESIAN_POINT('Ctrl Pts',(100.330244677677,-3.2228023996505,331.282276136441));
#57358=CARTESIAN_POINT('Ctrl Pts',(100.322484080585,-3.32371400817106,331.374795418961));
#57359=CARTESIAN_POINT('Ctrl Pts',(100.314731175224,-3.42452560054457,331.467223003189));
#57360=CARTESIAN_POINT('Ctrl Pts',(100.306978269863,-3.52158444591892,331.563955722731));
#57361=CARTESIAN_POINT('Ctrl Pts',(100.299225364503,-3.61450490775293,331.664653341206));
#57362=CARTESIAN_POINT('Ctrl Pts',(100.291478284049,-3.70735555666506,331.765275303632));
#57363=CARTESIAN_POINT('Ctrl Pts',(100.283731203594,-3.79607374631849,331.869855949245));
#57364=CARTESIAN_POINT('Ctrl Pts',(100.27598412314,-3.88030978721557,331.978017369716));
#57365=CARTESIAN_POINT('Ctrl Pts',(100.26824030382,-3.96451036893695,332.086133259618));
#57366=CARTESIAN_POINT('Ctrl Pts',(100.260496484501,-4.04423231438862,332.197826618326));
#57367=CARTESIAN_POINT('Ctrl Pts',(100.252752665181,-4.11916558285399,332.312685734133));
#57368=CARTESIAN_POINT('Ctrl Pts',(100.245010436373,-4.19408346069447,332.427521258903));
#57369=CARTESIAN_POINT('Ctrl Pts',(100.237268207565,-4.26421440410984,332.545520919834));
#57370=CARTESIAN_POINT('Ctrl Pts',(100.229525978757,-4.32929140183202,332.666243581579));
#57371=CARTESIAN_POINT('Ctrl Pts',(100.221783658601,-4.39436916737268,332.786967667684));
#57372=CARTESIAN_POINT('Ctrl Pts',(100.214041338445,-4.45439268265099,332.910414474062));
#57373=CARTESIAN_POINT('Ctrl Pts',(100.20629901829,-4.50914084844599,333.036118162573));
#57374=CARTESIAN_POINT('Ctrl Pts',(100.198554925221,-4.56390155101699,333.161850635956));
#57375=CARTESIAN_POINT('Ctrl Pts',(100.190810832152,-4.61338434413656,333.289840661015));
#57376=CARTESIAN_POINT('Ctrl Pts',(100.183066739084,-4.65741639196718,333.419602703642));
#57377=CARTESIAN_POINT('Ctrl Pts',(100.175314421007,-4.70149520627491,333.54950256665));
#57378=CARTESIAN_POINT('Ctrl Pts',(100.16756210293,-4.740111585229,333.681177835431));
#57379=CARTESIAN_POINT('Ctrl Pts',(100.159809784853,-4.77314253692811,333.814127584996));
#57380=CARTESIAN_POINT('Ctrl Pts',(100.152053284464,-4.80619130855539,333.947149059863));
#57381=CARTESIAN_POINT('Ctrl Pts',(100.144296784075,-4.83364857062412,334.081446002232));
#57382=CARTESIAN_POINT('Ctrl Pts',(100.136540283686,-4.85544274728425,334.216508589489));
#57383=CARTESIAN_POINT('Ctrl Pts',(100.128771457292,-4.87727155749343,334.351785807324));
#57384=CARTESIAN_POINT('Ctrl Pts',(100.121002630897,-4.89341925394935,334.487830712417));
#57385=CARTESIAN_POINT('Ctrl Pts',(100.113233804503,-4.90386622104369,334.624128813812));
#57386=CARTESIAN_POINT('Ctrl Pts',(100.106094995184,-4.91346598582958,334.749373748761));
#57387=CARTESIAN_POINT('Ctrl Pts',(100.098956185865,-4.91825274108658,334.874832226572));
#57388=CARTESIAN_POINT('Ctrl Pts',(100.091817376546,-4.91824999882167,335.00010765993));
#57389=CARTESIAN_POINT('',(98.3418173765424,-4.91824806724263,334.99563977476));
#57390=CARTESIAN_POINT('Ctrl Pts',(100.091817376508,-4.91824999882165,335.000107660602));
#57391=CARTESIAN_POINT('Ctrl Pts',(100.091491025897,-4.91824987345825,335.005834626047));
#57392=CARTESIAN_POINT('Ctrl Pts',(100.091164675285,-4.9182397451109,335.011561578566));
#57393=CARTESIAN_POINT('Ctrl Pts',(100.090838324674,-4.91821961388564,335.017288495902));
#57394=CARTESIAN_POINT('Ctrl Pts',(100.083063245895,-4.91774000129503,335.153728361095));
#57395=CARTESIAN_POINT('Ctrl Pts',(100.075288167117,-4.91157771429302,335.290363854516));
#57396=CARTESIAN_POINT('Ctrl Pts',(100.067513088339,-4.89970661782587,335.426682694439));
#57397=CARTESIAN_POINT('Ctrl Pts',(100.05974757729,-4.88785012949866,335.56283378535));
#57398=CARTESIAN_POINT('Ctrl Pts',(100.051982066241,-4.87029884313455,335.698668612402));
#57399=CARTESIAN_POINT('Ctrl Pts',(100.044216555192,-4.84707860505728,335.83367383244));
#57400=CARTESIAN_POINT('Ctrl Pts',(100.036458743669,-4.82388138991367,335.96854519441));
#57401=CARTESIAN_POINT('Ctrl Pts',(100.028700932147,-4.79502647455996,336.102588203565));
#57402=CARTESIAN_POINT('Ctrl Pts',(100.020943120625,-4.7605915543613,336.235293938722));
#57403=CARTESIAN_POINT('Ctrl Pts',(100.013191147102,-4.72618254753208,336.367899808605));
#57404=CARTESIAN_POINT('Ctrl Pts',(100.005439173579,-4.68620199180087,336.499170030741));
#57405=CARTESIAN_POINT('Ctrl Pts',(99.9976872000558,-4.64077871101077,336.628605543994));
#57406=CARTESIAN_POINT('Ctrl Pts',(99.9899385094982,-4.59537466700711,336.757986241231));
#57407=CARTESIAN_POINT('Ctrl Pts',(99.9821898189406,-4.54453261158466,336.885533406931));
#57408=CARTESIAN_POINT('Ctrl Pts',(99.9744411283829,-4.48843124733662,337.010763039354));
#57409=CARTESIAN_POINT('Ctrl Pts',(99.9666940500051,-4.43234155544598,337.135966616707));
#57410=CARTESIAN_POINT('Ctrl Pts',(99.9589469716273,-4.37099489096032,337.258853263387));
#57411=CARTESIAN_POINT('Ctrl Pts',(99.9511998932494,-4.30461798403781,337.378959241769));
#57412=CARTESIAN_POINT('Ctrl Pts',(99.9434527499436,-4.23824052081289,337.499066226755));
#57413=CARTESIAN_POINT('Ctrl Pts',(99.9357056066378,-4.16683292012931,337.616392154853));
#57414=CARTESIAN_POINT('Ctrl Pts',(99.927958463332,-4.09066753348094,337.730498524633));
#57415=CARTESIAN_POINT('Ctrl Pts',(99.9202095783039,-4.01448502323657,337.844630547949));
#57416=CARTESIAN_POINT('Ctrl Pts',(99.9124606932757,-3.93354281550278,337.955541247576));
#57417=CARTESIAN_POINT('Ctrl Pts',(99.9047118082476,-3.84815595032648,338.062822039307));
#57418=CARTESIAN_POINT('Ctrl Pts',(99.8969546984729,-3.76267845464938,338.170216699979));
#57419=CARTESIAN_POINT('Ctrl Pts',(99.8891975886981,-3.67274712147055,338.273973450068));
#57420=CARTESIAN_POINT('Ctrl Pts',(99.8814404789234,-3.57871692598314,338.373717271228));
#57421=CARTESIAN_POINT('Ctrl Pts',(99.8736792239972,-3.48463648376576,338.473514392296));
#57422=CARTESIAN_POINT('Ctrl Pts',(99.8659179690711,-3.38645309451952,338.569294038758));
#57423=CARTESIAN_POINT('Ctrl Pts',(99.8581567141449,-3.28455706248823,338.660719596713));
#57424=CARTESIAN_POINT('Ctrl Pts',(99.8503830437402,-3.18249803001352,338.752291405766));
#57425=CARTESIAN_POINT('Ctrl Pts',(99.8426093733356,-3.07671478859923,338.839494959173));
#57426=CARTESIAN_POINT('Ctrl Pts',(99.8348357029309,-2.96762973966714,338.92203477684));
#57427=CARTESIAN_POINT('Ctrl Pts',(99.8274238987539,-2.86362262600917,339.000732346135));
#57428=CARTESIAN_POINT('Ctrl Pts',(99.820012094577,-2.75661442154201,339.07519043785));
#57429=CARTESIAN_POINT('Ctrl Pts',(99.8126002904,-2.64699257541845,339.145191596076));
#57430=CARTESIAN_POINT('Ctrl Pts',(99.8048252116216,-2.5319978360677,339.21862371959));
#57431=CARTESIAN_POINT('Ctrl Pts',(99.7970501328432,-2.41376336757124,339.287383026617));
#57432=CARTESIAN_POINT('Ctrl Pts',(99.7892750540647,-2.29270581538381,339.351170314594));
#57433=CARTESIAN_POINT('Ctrl Pts',(99.7815095430157,-2.17179723222117,339.414879108253));
#57434=CARTESIAN_POINT('Ctrl Pts',(99.7737440319667,-2.0480728201003,339.473627876228));
#57435=CARTESIAN_POINT('Ctrl Pts',(99.7659785209177,-1.92197824715985,339.527160553807));
#57436=CARTESIAN_POINT('Ctrl Pts',(99.7582207093955,-1.79600869735567,339.58064015358));
#57437=CARTESIAN_POINT('Ctrl Pts',(99.7504628978733,-1.66767402088233,339.628913803307));
#57438=CARTESIAN_POINT('Ctrl Pts',(99.7427050863511,-1.53744422584185,339.671771432222));
#57439=CARTESIAN_POINT('Ctrl Pts',(99.7349531128281,-1.40731243285197,339.714596809412));
#57440=CARTESIAN_POINT('Ctrl Pts',(99.7272011393051,-1.27528872974119,339.752014156631));
#57441=CARTESIAN_POINT('Ctrl Pts',(99.7194491657821,-1.14186250163802,339.783861733982));
#57442=CARTESIAN_POINT('Ctrl Pts',(99.7117004752245,-1.00849277962175,339.815695823864));
#57443=CARTESIAN_POINT('Ctrl Pts',(99.7039517846669,-0.873722093380531,
339.841964744806));
#57444=CARTESIAN_POINT('Ctrl Pts',(99.6962030941093,-0.73805415652861,339.862556850519));
#57445=CARTESIAN_POINT('Ctrl Pts',(99.6884560157314,-0.60241444652398,339.883144671873));
#57446=CARTESIAN_POINT('Ctrl Pts',(99.6807089373536,-0.465878243434824,
339.898057968686));
#57447=CARTESIAN_POINT('Ctrl Pts',(99.6729618589758,-0.328958210823053,
339.907236448148));
#57448=CARTESIAN_POINT('Ctrl Pts',(99.6652147156699,-0.192037030689624,
339.916415004534));
#57449=CARTESIAN_POINT('Ctrl Pts',(99.6574675723642,-0.0547324046163078,
339.919858621559));
#57450=CARTESIAN_POINT('Ctrl Pts',(99.6497204290583,0.0824395371690725,
339.91755902712));
#57451=CARTESIAN_POINT('Ctrl Pts',(99.6419715440303,0.219642318119116,339.915258915683));
#57452=CARTESIAN_POINT('Ctrl Pts',(99.6342226590022,0.356711964679367,339.907213029997));
#57453=CARTESIAN_POINT('Ctrl Pts',(99.6264737739741,0.49313440342502,339.893465185598));
#57454=CARTESIAN_POINT('Ctrl Pts',(99.6187166641994,0.629701642356758,339.879702749095));
#57455=CARTESIAN_POINT('Ctrl Pts',(99.6109595544246,0.765619911701912,339.860226303458));
#57456=CARTESIAN_POINT('Ctrl Pts',(99.6032024446499,0.900381753085704,339.835131410956));
#57457=CARTESIAN_POINT('Ctrl Pts',(99.5954411897237,1.03521560688868,339.810023108545));
#57458=CARTESIAN_POINT('Ctrl Pts',(99.5876799347976,1.16889142064978,339.779290464412));
#57459=CARTESIAN_POINT('Ctrl Pts',(99.5799186798714,1.30091491253837,339.743079532628));
#57460=CARTESIAN_POINT('Ctrl Pts',(99.5721450094668,1.43314959898763,339.706810675154));
#57461=CARTESIAN_POINT('Ctrl Pts',(99.5643713390621,1.56372630922448,339.66504613715));
#57462=CARTESIAN_POINT('Ctrl Pts',(99.5565976686574,1.6921679820863,339.617981223749));
#57463=CARTESIAN_POINT('Ctrl Pts',(99.5491858644803,1.81463066417573,339.57310719339));
#57464=CARTESIAN_POINT('Ctrl Pts',(99.5417740603032,1.93515234156217,339.523415257164));
#57465=CARTESIAN_POINT('Ctrl Pts',(99.5343622561261,2.05334047996373,339.46911355146));
#57466=CARTESIAN_POINT('Ctrl Pts',(99.5265871773476,2.17732137109212,339.412150357403));
#57467=CARTESIAN_POINT('Ctrl Pts',(99.5188120985692,2.29912599448184,339.349934076862));
#57468=CARTESIAN_POINT('Ctrl Pts',(99.5110370197908,2.41827727355382,339.282653160217));
#57469=CARTESIAN_POINT('Ctrl Pts',(99.5032715087417,2.53728192939135,339.215455037022));
#57470=CARTESIAN_POINT('Ctrl Pts',(99.4955059976928,2.65363940043506,339.14320486868));
#57471=CARTESIAN_POINT('Ctrl Pts',(99.4877404866437,2.76689317980419,339.066138855727));
#57472=CARTESIAN_POINT('Ctrl Pts',(99.4799826751215,2.88003466772134,338.98914925395));
#57473=CARTESIAN_POINT('Ctrl Pts',(99.4722248635993,2.99007826693166,338.907353528412));
#57474=CARTESIAN_POINT('Ctrl Pts',(99.4644670520771,3.09659297609416,338.821033237608));
#57475=CARTESIAN_POINT('Ctrl Pts',(99.4567150785541,3.20302752956024,338.73477790556));
#57476=CARTESIAN_POINT('Ctrl Pts',(99.4489631050311,3.30593817637274,338.644005030599));
#57477=CARTESIAN_POINT('Ctrl Pts',(99.4412111315081,3.40492407162688,338.549038620381));
#57478=CARTESIAN_POINT('Ctrl Pts',(99.4334624409505,3.50386804629555,338.454112428494));
#57479=CARTESIAN_POINT('Ctrl Pts',(99.4257137503929,3.59889029380429,338.35499650366));
#57480=CARTESIAN_POINT('Ctrl Pts',(99.4179650598353,3.68962434006682,338.252054011188));
#57481=CARTESIAN_POINT('Ctrl Pts',(99.4102179814574,3.78033950835326,338.149132936762));
#57482=CARTESIAN_POINT('Ctrl Pts',(99.4024709030796,3.86676799174228,338.042387171343));
#57483=CARTESIAN_POINT('Ctrl Pts',(99.3947238247018,3.94858165705209,337.932215196757));
#57484=CARTESIAN_POINT('Ctrl Pts',(99.386976681396,4.03039600803916,337.822042298823));
#57485=CARTESIAN_POINT('Ctrl Pts',(99.3792295380902,4.10759523076798,337.70844344826));
#57486=CARTESIAN_POINT('Ctrl Pts',(99.3714823947844,4.17989306136877,337.591848193475));
#57487=CARTESIAN_POINT('Ctrl Pts',(99.3637335097563,4.25220714605676,337.475226725603));
#57488=CARTESIAN_POINT('Ctrl Pts',(99.3559846247281,4.31961743994021,337.35560784514));
#57489=CARTESIAN_POINT('Ctrl Pts',(99.3482357397,4.38188259381066,337.233447558498));
#57490=CARTESIAN_POINT('Ctrl Pts',(99.3404786299253,4.44421383655879,337.111157609665));
#57491=CARTESIAN_POINT('Ctrl Pts',(99.3327215201506,4.50138885244284,336.986321214992));
#57492=CARTESIAN_POINT('Ctrl Pts',(99.3249644103759,4.55321338696688,336.859416821276));
#57493=CARTESIAN_POINT('Ctrl Pts',(99.3172031554497,4.60506561486511,336.732444613911));
#57494=CARTESIAN_POINT('Ctrl Pts',(99.3094419005235,4.65156153190451,336.603402573092));
#57495=CARTESIAN_POINT('Ctrl Pts',(99.3016806455974,4.69255647380802,336.472785389194));
#57496=CARTESIAN_POINT('Ctrl Pts',(99.2939069751927,4.73361699425838,336.341959260369));
#57497=CARTESIAN_POINT('Ctrl Pts',(99.2861333047881,4.76915885364278,336.209553331037));
#57498=CARTESIAN_POINT('Ctrl Pts',(99.2783596343834,4.79908812304527,336.076074462919));
#57499=CARTESIAN_POINT('Ctrl Pts',(99.2709478302064,4.82762417775645,335.948809068225));
#57500=CARTESIAN_POINT('Ctrl Pts',(99.2635360260293,4.85105836361912,335.82056866048));
#57501=CARTESIAN_POINT('Ctrl Pts',(99.2561242218522,4.86935328413904,335.691795964678));
#57502=CARTESIAN_POINT('Ctrl Pts',(99.2483491430738,4.88854489321143,335.55671173546));
#57503=CARTESIAN_POINT('Ctrl Pts',(99.2405740642953,4.90214136644291,335.420614829694));
#57504=CARTESIAN_POINT('Ctrl Pts',(99.2327989855169,4.91004300226502,335.284008412566));
#57505=CARTESIAN_POINT('Ctrl Pts',(99.2250334744679,4.91793491462121,335.147570098331));
#57506=CARTESIAN_POINT('Ctrl Pts',(99.2172679634189,4.92014591084444,335.010623906749));
#57507=CARTESIAN_POINT('Ctrl Pts',(99.2095024523699,4.91662757493826,334.873681545859));
#57508=CARTESIAN_POINT('Ctrl Pts',(99.2017446408477,4.91311272747239,334.736874963717));
#57509=CARTESIAN_POINT('Ctrl Pts',(99.1939868293255,4.90387986266518,334.600072592938));
#57510=CARTESIAN_POINT('Ctrl Pts',(99.1862290178033,4.88893250950576,334.4637892392));
#57511=CARTESIAN_POINT('Ctrl Pts',(99.1784770442803,4.87399640470359,334.327608443008));
#57512=CARTESIAN_POINT('Ctrl Pts',(99.1707250707573,4.85335441359659,334.191946273413));
#57513=CARTESIAN_POINT('Ctrl Pts',(99.1629730972343,4.82706208095634,334.057315148582));
#57514=CARTESIAN_POINT('Ctrl Pts',(99.1552244066766,4.80078088313457,333.922741040112));
#57515=CARTESIAN_POINT('Ctrl Pts',(99.147475716119,4.76885417789806,333.789197490772));
#57516=CARTESIAN_POINT('Ctrl Pts',(99.1397270255614,4.73138903854832,333.657189206029));
#57517=CARTESIAN_POINT('Ctrl Pts',(99.1319799471835,4.69393169413374,333.525208386712));
#57518=CARTESIAN_POINT('Ctrl Pts',(99.1242328688057,4.65093831429878,333.39476257242));
#57519=CARTESIAN_POINT('Ctrl Pts',(99.1164857904279,4.60256641921949,333.266343338728));
#57520=CARTESIAN_POINT('Ctrl Pts',(99.1087386471221,4.55419411873716,333.137923028759));
#57521=CARTESIAN_POINT('Ctrl Pts',(99.1009915038163,4.50044335088185,333.011529699052));
#57522=CARTESIAN_POINT('Ctrl Pts',(99.0932443605105,4.44152041826989,332.887636528295));
#57523=CARTESIAN_POINT('Ctrl Pts',(99.0854954754823,4.3825842385317,332.763715503724));
#57524=CARTESIAN_POINT('Ctrl Pts',(99.0777465904543,4.31847374801572,332.642296109513));
#57525=CARTESIAN_POINT('Ctrl Pts',(99.0699977054262,4.24944180433612,332.523828072597));
#57526=CARTESIAN_POINT('Ctrl Pts',(99.0622405956514,4.18033658943827,332.405234292482));
#57527=CARTESIAN_POINT('Ctrl Pts',(99.0544834858767,4.10629968368623,332.289598465581));
#57528=CARTESIAN_POINT('Ctrl Pts',(99.046726376102,4.02762830094663,332.17734285966));
#57529=CARTESIAN_POINT('Ctrl Pts',(99.0389651211758,3.94891487873553,332.065027267932));
#57530=CARTESIAN_POINT('Ctrl Pts',(99.0312038662496,3.86556228226477,331.956095806629));
#57531=CARTESIAN_POINT('Ctrl Pts',(99.0234426113235,3.77790822108268,331.850937832374));
#57532=CARTESIAN_POINT('Ctrl Pts',(99.0156689409188,3.69011394196909,331.745611639631));
#57533=CARTESIAN_POINT('Ctrl Pts',(99.0078952705141,3.59800471074091,331.644071286009));
#57534=CARTESIAN_POINT('Ctrl Pts',(99.0001216001095,3.50195592790865,331.546670050301));
#57535=CARTESIAN_POINT('Ctrl Pts',(98.9927097959324,3.41037823902563,331.453802865549));
#57536=CARTESIAN_POINT('Ctrl Pts',(98.9852979917553,3.3152197268874,331.364698315647));
#57537=CARTESIAN_POINT('Ctrl Pts',(98.9778861875783,3.21683245099812,331.279627432003));
#57538=CARTESIAN_POINT('Ctrl Pts',(98.9701111087999,3.11362292163643,331.190386970938));
#57539=CARTESIAN_POINT('Ctrl Pts',(98.9623360300214,3.0065339619087,331.10530356158));
#57540=CARTESIAN_POINT('Ctrl Pts',(98.954560951243,2.89593473991489,331.024733336661));
#57541=CARTESIAN_POINT('Ctrl Pts',(98.946795440194,2.78547161730484,330.944262258533));
#57542=CARTESIAN_POINT('Ctrl Pts',(98.939029929145,2.67150714010772,330.868293542403));
#57543=CARTESIAN_POINT('Ctrl Pts',(98.9312644180959,2.55444541385672,330.797144816898));
#57544=CARTESIAN_POINT('Ctrl Pts',(98.9235066065738,2.43749975464812,330.726066635562));
#57545=CARTESIAN_POINT('Ctrl Pts',(98.9157487950515,2.31746328958002,330.659799136005));
#57546=CARTESIAN_POINT('Ctrl Pts',(98.9079909835293,2.19477083947044,330.59861794152));
#57547=CARTESIAN_POINT('Ctrl Pts',(98.9002390100063,2.07217071932036,330.537482787824));
#57548=CARTESIAN_POINT('Ctrl Pts',(98.8924870364833,1.94691894085738,330.481426494262));
#57549=CARTESIAN_POINT('Ctrl Pts',(98.8847350629603,1.81947646591242,330.430679650923));
#57550=CARTESIAN_POINT('Ctrl Pts',(98.8769863724027,1.69208796293135,330.379954298902));
#57551=CARTESIAN_POINT('Ctrl Pts',(98.869237681845,1.56251097110767,330.334534069187));
#57552=CARTESIAN_POINT('Ctrl Pts',(98.8614889912874,1.43122785154232,330.294602046642));
#57553=CARTESIAN_POINT('Ctrl Pts',(98.8537419129096,1.29997204652649,330.254678332287));
#57554=CARTESIAN_POINT('Ctrl Pts',(98.8459948345317,1.16701119356086,330.220240667521));
#57555=CARTESIAN_POINT('Ctrl Pts',(98.8382477561539,1.03284391223874,330.191422610017));
#57556=CARTESIAN_POINT('Ctrl Pts',(98.8305006128481,0.898675506465665,330.162604310991));
#57557=CARTESIAN_POINT('Ctrl Pts',(98.8227534695423,0.763301034327023,330.139405795251));
#57558=CARTESIAN_POINT('Ctrl Pts',(98.8150063262365,0.627230044059254,330.121909642664));
#57559=CARTESIAN_POINT('Ctrl Pts',(98.8072574412084,0.491128462143912,330.104409556572));
#57560=CARTESIAN_POINT('Ctrl Pts',(98.7995085561803,0.354330438105604,330.092614434533));
#57561=CARTESIAN_POINT('Ctrl Pts',(98.7917596711522,0.217350992680787,330.086555016235));
#57562=CARTESIAN_POINT('Ctrl Pts',(98.7840025613775,0.0802261558574262,
330.080489166408));
#57563=CARTESIAN_POINT('Ctrl Pts',(98.7762454516027,-0.0570800959049829,
330.080171198845));
#57564=CARTESIAN_POINT('Ctrl Pts',(98.768488341828,-0.194051829155775,330.085579693382));
#57565=CARTESIAN_POINT('Ctrl Pts',(98.7607270869018,-0.33109675572131,330.090991078045));
#57566=CARTESIAN_POINT('Ctrl Pts',(98.7529658319757,-0.467806418203325,
330.10213499047));
#57567=CARTESIAN_POINT('Ctrl Pts',(98.7452045770495,-0.603670644296039,
330.118938146703));
#57568=CARTESIAN_POINT('Ctrl Pts',(98.7374309066448,-0.739752208872452,
330.135768182509));
#57569=CARTESIAN_POINT('Ctrl Pts',(98.7296572362401,-0.874985248745111,
330.158275488384));
#57570=CARTESIAN_POINT('Ctrl Pts',(98.7218835658355,-1.00886953348464,330.186335561456));
#57571=CARTESIAN_POINT('Ctrl Pts',(98.7144717616583,-1.1365214725594,330.213089431375));
#57572=CARTESIAN_POINT('Ctrl Pts',(98.7070599574813,-1.26294712064762,330.24489066958));
#57573=CARTESIAN_POINT('Ctrl Pts',(98.6996481533041,-1.38772804205732,330.28158989237));
#57574=CARTESIAN_POINT('Ctrl Pts',(98.6918730745257,-1.5186248481281,330.32008785339));
#57575=CARTESIAN_POINT('Ctrl Pts',(98.6840979957473,-1.64812528310341,330.36409772938));
#57576=CARTESIAN_POINT('Ctrl Pts',(98.6763229169688,-1.77573008933132,330.413501802863));
#57577=CARTESIAN_POINT('Ctrl Pts',(98.6685574059198,-1.90317786972135,330.462845081488));
#57578=CARTESIAN_POINT('Ctrl Pts',(98.6607918948708,-2.0287343017279,330.517569210307));
#57579=CARTESIAN_POINT('Ctrl Pts',(98.6530263838218,-2.15191359997138,330.57750625543));
#57580=CARTESIAN_POINT('Ctrl Pts',(98.6452685722996,-2.27497076558185,330.637383872799));
#57581=CARTESIAN_POINT('Ctrl Pts',(98.6375107607774,-2.39565513865294,330.702463950702));
#57582=CARTESIAN_POINT('Ctrl Pts',(98.6297529492552,-2.5134996351845,330.772529994615));
#57583=CARTESIAN_POINT('Ctrl Pts',(98.6220009757322,-2.63125544999552,330.842543311609));
#57584=CARTESIAN_POINT('Ctrl Pts',(98.6142490022092,-2.74617530743215,330.917534927292));
#57585=CARTESIAN_POINT('Ctrl Pts',(98.6064970286862,-2.85781584647261,330.997241994556));
#57586=CARTESIAN_POINT('Ctrl Pts',(98.5987483381286,-2.9694091056785,331.076915305828));
#57587=CARTESIAN_POINT('Ctrl Pts',(98.5909996475709,-3.07772549124603,331.161299870146));
#57588=CARTESIAN_POINT('Ctrl Pts',(98.5832509570133,-3.18235000993756,331.250089137493));
#57589=CARTESIAN_POINT('Ctrl Pts',(98.5755038786355,-3.28695276062421,331.338859931491));
#57590=CARTESIAN_POINT('Ctrl Pts',(98.5677568002576,-3.387864874453,331.432033352908));
#57591=CARTESIAN_POINT('Ctrl Pts',(98.5600097218798,-3.48470420825454,331.52926237761));
#57592=CARTESIAN_POINT('Ctrl Pts',(98.5522625785739,-3.5815443536629,331.626492217185));
#57593=CARTESIAN_POINT('Ctrl Pts',(98.5445154352681,-3.67431137512724,331.727777450897));
#57594=CARTESIAN_POINT('Ctrl Pts',(98.5367682919623,-3.76266008368666,331.832734277467));
#57595=CARTESIAN_POINT('Ctrl Pts',(98.5290194069342,-3.85102865491146,331.93771470056));
#57596=CARTESIAN_POINT('Ctrl Pts',(98.5212705219061,-3.93497668494761,332.046368060093));
#57597=CARTESIAN_POINT('Ctrl Pts',(98.513521636878,-4.01419961686452,332.158277899149));
#57598=CARTESIAN_POINT('Ctrl Pts',(98.5057645271033,-4.09350663681984,332.270306520464));
#57599=CARTESIAN_POINT('Ctrl Pts',(98.4980074173285,-4.16807831398719,332.385598206378));
#57600=CARTESIAN_POINT('Ctrl Pts',(98.4902503075538,-4.23765345984436,332.503707505766));
#57601=CARTESIAN_POINT('Ctrl Pts',(98.4824890526276,-4.3072657844349,332.621879918987));
#57602=CARTESIAN_POINT('Ctrl Pts',(98.4747277977014,-4.37187607349971,332.742872601191));
#57603=CARTESIAN_POINT('Ctrl Pts',(98.4669665427753,-4.43126986957041,332.866216879452));
#57604=CARTESIAN_POINT('Ctrl Pts',(98.4591928723706,-4.49075867635843,332.989758468359));
#57605=CARTESIAN_POINT('Ctrl Pts',(98.451419201966,-4.54501416022077,333.115658811337));
#57606=CARTESIAN_POINT('Ctrl Pts',(98.4436455315613,-4.59387031489085,333.243429878296));
#57607=CARTESIAN_POINT('Ctrl Pts',(98.4362337273843,-4.6404522038063,333.365253171346));
#57608=CARTESIAN_POINT('Ctrl Pts',(98.4288219232073,-4.68212603663192,333.488776670742));
#57609=CARTESIAN_POINT('Ctrl Pts',(98.4214101190303,-4.71879099374629,333.61356766489));
#57610=CARTESIAN_POINT('Ctrl Pts',(98.4117633154176,-4.76651211971021,333.775988876302));
#57611=CARTESIAN_POINT('Ctrl Pts',(98.4021165118049,-4.80587145811916,333.940970878287));
#57612=CARTESIAN_POINT('Ctrl Pts',(98.3924697081922,-4.83663764127717,334.107744773352));
#57613=CARTESIAN_POINT('Ctrl Pts',(98.3829601260023,-4.86696618938061,334.272146385112));
#57614=CARTESIAN_POINT('Ctrl Pts',(98.3734505438124,-4.88894431319201,334.438289332985));
#57615=CARTESIAN_POINT('Ctrl Pts',(98.3639409616224,-4.90239600787342,334.605416112231));
#57616=CARTESIAN_POINT('Ctrl Pts',(98.3565664332624,-4.9128275811999,334.735020247161));
#57617=CARTESIAN_POINT('Ctrl Pts',(98.3491919049024,-4.91813244098066,334.865215631944));
#57618=CARTESIAN_POINT('Ctrl Pts',(98.3418173765424,-4.91824806724263,334.99563977476));
#57619=CARTESIAN_POINT('',(96.5918173764665,-4.91824959781138,335.001989001811));
#57620=CARTESIAN_POINT('Ctrl Pts',(98.3418173765085,-4.91824806724316,334.995639775358));
#57621=CARTESIAN_POINT('Ctrl Pts',(98.3341262128526,-4.91836865805767,335.131663854203));
#57622=CARTESIAN_POINT('Ctrl Pts',(98.3264350491966,-4.91284197471611,335.267801370545));
#57623=CARTESIAN_POINT('Ctrl Pts',(98.3187438855406,-4.9016666356082,335.403543375445));
#57624=CARTESIAN_POINT('Ctrl Pts',(98.3110556037903,-4.89049548393849,335.539234517346));
#57625=CARTESIAN_POINT('Ctrl Pts',(98.3033673220399,-4.87367991624643,335.674530046989));
#57626=CARTESIAN_POINT('Ctrl Pts',(98.2956790402896,-4.85127061813189,335.808923019916));
#57627=CARTESIAN_POINT('Ctrl Pts',(98.287992039792,-4.82886505452859,335.943293596244));
#57628=CARTESIAN_POINT('Ctrl Pts',(98.2803050392944,-4.80086767947502,336.076761523036));
#57629=CARTESIAN_POINT('Ctrl Pts',(98.2726180387968,-4.7673807476608,336.208827477076));
#57630=CARTESIAN_POINT('Ctrl Pts',(98.2649305918404,-4.73389187093554,336.340901101467));
#57631=CARTESIAN_POINT('Ctrl Pts',(98.2572431448842,-4.69491290094729,336.471572205827));
#57632=CARTESIAN_POINT('Ctrl Pts',(98.2495556979278,-4.65059654726642,336.600354591037));
#57633=CARTESIAN_POINT('Ctrl Pts',(98.2418660767841,-4.60626765989809,336.729173398878));
#57634=CARTESIAN_POINT('Ctrl Pts',(98.2341764556405,-4.55659851553014,336.856102049364));
#57635=CARTESIAN_POINT('Ctrl Pts',(98.2264868344968,-4.50179056263719,336.980672813125));
#57636=CARTESIAN_POINT('Ctrl Pts',(98.2187888072795,-4.44692269525984,337.105379754076));
#57637=CARTESIAN_POINT('Ctrl Pts',(98.2110907800621,-4.38690496302017,337.227723297566));
#57638=CARTESIAN_POINT('Ctrl Pts',(98.2033927528448,-4.32198570563955,337.347258533427));
#57639=CARTESIAN_POINT('Ctrl Pts',(98.1956901004697,-4.25702744322512,337.466865588901));
#57640=CARTESIAN_POINT('Ctrl Pts',(98.1879874480945,-4.18716199483521,337.583660636348));
#57641=CARTESIAN_POINT('Ctrl Pts',(98.1802847957194,-4.11268127752368,337.697227423115));
#57642=CARTESIAN_POINT('Ctrl Pts',(98.172570452277,-4.03808751355848,337.810966581279));
#57643=CARTESIAN_POINT('Ctrl Pts',(98.1648561088346,-3.95886472363139,337.921467372271));
#57644=CARTESIAN_POINT('Ctrl Pts',(98.1571417653922,-3.87534569531122,338.028345885848));
#57645=CARTESIAN_POINT('Ctrl Pts',(98.1524852051803,-3.82493163387864,338.092860285233));
#57646=CARTESIAN_POINT('Ctrl Pts',(98.1478286449683,-3.77295293558199,338.156055549211));
#57647=CARTESIAN_POINT('Ctrl Pts',(98.1431720847564,-3.71948909971673,338.217853927634));
#57648=CARTESIAN_POINT('Ctrl Pts',(98.1353970059779,-3.63022030113384,338.321038948067));
#57649=CARTESIAN_POINT('Ctrl Pts',(98.1276219271995,-3.53651339248321,338.420669501185));
#57650=CARTESIAN_POINT('Ctrl Pts',(98.119846848421,-3.43868235447085,338.516339961885));
#57651=CARTESIAN_POINT('Ctrl Pts',(98.112081337372,-3.34097170377907,338.611892693993));
#57652=CARTESIAN_POINT('Ctrl Pts',(98.104315826323,-3.23914729831483,338.703494759172));
#57653=CARTESIAN_POINT('Ctrl Pts',(98.096550315274,-3.13356324130191,338.790773598523));
#57654=CARTESIAN_POINT('Ctrl Pts',(98.0887925037518,-3.02808387118892,338.877965900651));
#57655=CARTESIAN_POINT('Ctrl Pts',(98.0810346922296,-2.9188525672001,338.960843259878));
#57656=CARTESIAN_POINT('Ctrl Pts',(98.0732768807074,-2.80625988167974,339.039070256752));
#57657=CARTESIAN_POINT('Ctrl Pts',(98.0655249071844,-2.69375192572582,339.117238385329));
#57658=CARTESIAN_POINT('Ctrl Pts',(98.0577729336614,-2.57788794288802,339.190762895099));
#57659=CARTESIAN_POINT('Ctrl Pts',(98.0500209601384,-2.45909084455753,339.259349161634));
#57660=CARTESIAN_POINT('Ctrl Pts',(98.0422722695808,-2.34034405686871,339.327906381844));
#57661=CARTESIAN_POINT('Ctrl Pts',(98.0345235790232,-2.21866696209217,339.391529323337));
#57662=CARTESIAN_POINT('Ctrl Pts',(98.0267748884656,-2.09451049475174,339.449967286383));
#57663=CARTESIAN_POINT('Ctrl Pts',(98.0190278100877,-1.97037985920131,339.508393090922));
#57664=CARTESIAN_POINT('Ctrl Pts',(98.0112807317099,-1.84377123059323,339.561635896425));
#57665=CARTESIAN_POINT('Ctrl Pts',(98.0035336533321,-1.71515877093141,339.609491669696));
#57666=CARTESIAN_POINT('Ctrl Pts',(97.9957865100263,-1.5865452333732,339.657347844045));
#57667=CARTESIAN_POINT('Ctrl Pts',(97.9880393667205,-1.45592819760025,339.699816759798));
#57668=CARTESIAN_POINT('Ctrl Pts',(97.9802922234147,-1.32379998799317,339.736743253997));
#57669=CARTESIAN_POINT('Ctrl Pts',(97.9725433383866,-1.19164207315978,339.773678050056));
#57670=CARTESIAN_POINT('Ctrl Pts',(97.9647944533585,-1.05797268481536,339.805067839865));
#57671=CARTESIAN_POINT('Ctrl Pts',(97.9570455683304,-0.923297034851003,
339.830807970509));
#57672=CARTESIAN_POINT('Ctrl Pts',(97.9492884585557,-0.788478438760129,
339.856575421994));
#57673=CARTESIAN_POINT('Ctrl Pts',(97.9415313487809,-0.652651832037589,
339.876681162036));
#57674=CARTESIAN_POINT('Ctrl Pts',(97.9337742390062,-0.516330847990964,
339.891072021338));
#57675=CARTESIAN_POINT('Ctrl Pts',(97.92601298408,-0.379937018369072,339.905470570654));
#57676=CARTESIAN_POINT('Ctrl Pts',(97.9182517291539,-0.243048674915173,
339.914148129444));
#57677=CARTESIAN_POINT('Ctrl Pts',(97.9104904742277,-0.106181225512197,
339.917103681015));
#57678=CARTESIAN_POINT('Ctrl Pts',(97.902716803823,0.03090516720492,339.920063960505));
#57679=CARTESIAN_POINT('Ctrl Pts',(97.8949431334184,0.16797020808126,339.917283949611));
#57680=CARTESIAN_POINT('Ctrl Pts',(97.8871694630137,0.304500944683629,339.908814748713));
#57681=CARTESIAN_POINT('Ctrl Pts',(97.8797576588366,0.434676142649488,339.900739791156));
#57682=CARTESIAN_POINT('Ctrl Pts',(97.8723458546596,0.564365374310985,339.887493416679));
#57683=CARTESIAN_POINT('Ctrl Pts',(97.8649340504825,0.693133041553943,339.869163136434));
#57684=CARTESIAN_POINT('Ctrl Pts',(97.857158971704,0.828211995747758,339.849934434551));
#57685=CARTESIAN_POINT('Ctrl Pts',(97.8493838929256,0.96270363856121,339.825050105009));
#57686=CARTESIAN_POINT('Ctrl Pts',(97.8416088141472,1.09609695821608,339.794554673866));
#57687=CARTESIAN_POINT('Ctrl Pts',(97.8338433030982,1.22932612889878,339.764096769292));
#57688=CARTESIAN_POINT('Ctrl Pts',(97.8260777920492,1.36145928823187,339.728041588002));
#57689=CARTESIAN_POINT('Ctrl Pts',(97.8183122810002,1.49199151791639,339.686485289955));
#57690=CARTESIAN_POINT('Ctrl Pts',(97.810554469478,1.62239432451515,339.644970195098));
#57691=CARTESIAN_POINT('Ctrl Pts',(97.8027966579558,1.75119899027894,339.597964955806));
#57692=CARTESIAN_POINT('Ctrl Pts',(97.7950388464336,1.8779121035515,339.545616481165));
#57693=CARTESIAN_POINT('Ctrl Pts',(97.7872868729105,2.00452986118854,339.49330740041));
#57694=CARTESIAN_POINT('Ctrl Pts',(97.7795348993875,2.12905883941901,339.435663236464));
#57695=CARTESIAN_POINT('Ctrl Pts',(97.7717829258645,2.25102242065511,339.372880186354));
#57696=CARTESIAN_POINT('Ctrl Pts',(97.7640342353068,2.37293435024156,339.310123724903));
#57697=CARTESIAN_POINT('Ctrl Pts',(97.7562855447492,2.49228269689234,339.242232884364));
#57698=CARTESIAN_POINT('Ctrl Pts',(97.7485368541916,2.60861261531108,339.169451197189));
#57699=CARTESIAN_POINT('Ctrl Pts',(97.7407897758138,2.72491833031869,339.096684652852));
#57700=CARTESIAN_POINT('Ctrl Pts',(97.733042697436,2.83820653509296,339.019029493108));
#57701=CARTESIAN_POINT('Ctrl Pts',(97.7252956190581,2.9480490574991,338.936774036833));
#57702=CARTESIAN_POINT('Ctrl Pts',(97.7175484757523,3.05789250049152,338.854517891177));
#57703=CARTESIAN_POINT('Ctrl Pts',(97.7098013324465,3.16428989064397,338.767661606384));
#57704=CARTESIAN_POINT('Ctrl Pts',(97.7020541891407,3.26684432314165,338.676535220946));
#57705=CARTESIAN_POINT('Ctrl Pts',(97.6943053041126,3.36942181205292,338.585388348363));
#57706=CARTESIAN_POINT('Ctrl Pts',(97.6865564190845,3.46815433195597,338.489969724404));
#57707=CARTESIAN_POINT('Ctrl Pts',(97.6788075340564,3.56268047883941,338.39064755883));
#57708=CARTESIAN_POINT('Ctrl Pts',(97.6710504242817,3.65730695675178,338.291219971683));
#57709=CARTESIAN_POINT('Ctrl Pts',(97.663293314507,3.74771787311701,338.18788084996));
#57710=CARTESIAN_POINT('Ctrl Pts',(97.6555362047322,3.83359056028304,338.08103334591));
#57711=CARTESIAN_POINT('Ctrl Pts',(97.647774949806,3.91950913506754,337.97412874597));
#57712=CARTESIAN_POINT('Ctrl Pts',(97.6400136948799,4.00088441667551,337.863712342554));
#57713=CARTESIAN_POINT('Ctrl Pts',(97.6322524399537,4.07743663337025,337.750217002956));
#57714=CARTESIAN_POINT('Ctrl Pts',(97.624478769549,4.15411130866329,337.636540107804));
#57715=CARTESIAN_POINT('Ctrl Pts',(97.6167050991444,4.22594729660149,337.519774767365));
#57716=CARTESIAN_POINT('Ctrl Pts',(97.6089314287397,4.29270998059204,337.400379987632));
#57717=CARTESIAN_POINT('Ctrl Pts',(97.6015196245627,4.35636484558052,337.286543063621));
#57718=CARTESIAN_POINT('Ctrl Pts',(97.5941078203856,4.41540797150253,337.170316248613));
#57719=CARTESIAN_POINT('Ctrl Pts',(97.5866960162085,4.46967722121733,337.052113203659));
#57720=CARTESIAN_POINT('Ctrl Pts',(97.5789209374301,4.5266063685206,336.928116675363));
#57721=CARTESIAN_POINT('Ctrl Pts',(97.5711458586516,4.57846174998048,336.80155344509));
#57722=CARTESIAN_POINT('Ctrl Pts',(97.5633707798732,4.62500427071286,336.672877329151));
#57723=CARTESIAN_POINT('Ctrl Pts',(97.5556052688242,4.67148951791053,336.544359557365));
#57724=CARTESIAN_POINT('Ctrl Pts',(97.5478397577751,4.71267478107494,336.413734437302));
#57725=CARTESIAN_POINT('Ctrl Pts',(97.5400742467261,4.7483676829023,336.281478603204));
#57726=CARTESIAN_POINT('Ctrl Pts',(97.5323164352039,4.7840251951135,336.14935390115));
#57727=CARTESIAN_POINT('Ctrl Pts',(97.5245586236817,4.81420108203467,336.015602077641));
#57728=CARTESIAN_POINT('Ctrl Pts',(97.5168008121595,4.83875186929176,335.880717554001));
#57729=CARTESIAN_POINT('Ctrl Pts',(97.5090488386364,4.86328418130292,335.745934535242));
#57730=CARTESIAN_POINT('Ctrl Pts',(97.5012968651134,4.88219974964813,335.610020896007));
#57731=CARTESIAN_POINT('Ctrl Pts',(97.4935448915904,4.89540563546843,335.473483607661));
#57732=CARTESIAN_POINT('Ctrl Pts',(97.4857962010328,4.90860592858823,335.337004142939));
#57733=CARTESIAN_POINT('Ctrl Pts',(97.4780475104752,4.91610131097061,335.199901942663));
#57734=CARTESIAN_POINT('Ctrl Pts',(97.4702988199175,4.9178504313616,335.062691285332));
#57735=CARTESIAN_POINT('Ctrl Pts',(97.4625517415397,4.91959918783348,334.925509175824));
#57736=CARTESIAN_POINT('Ctrl Pts',(97.4548046631618,4.91560405538378,334.788219044742));
#57737=CARTESIAN_POINT('Ctrl Pts',(97.447057584784,4.90587577899509,334.651336977055));
#57738=CARTESIAN_POINT('Ctrl Pts',(97.4393104414782,4.89614742107409,334.514453762165));
#57739=CARTESIAN_POINT('Ctrl Pts',(97.4315632981724,4.88068585108596,334.377979007382));
#57740=CARTESIAN_POINT('Ctrl Pts',(97.4238161548666,4.85955381747202,334.242425081201));
#57741=CARTESIAN_POINT('Ctrl Pts',(97.4160672698385,4.83841703292822,334.106840679619));
#57742=CARTESIAN_POINT('Ctrl Pts',(97.4083183848103,4.81160730816411,333.972177904722));
#57743=CARTESIAN_POINT('Ctrl Pts',(97.4005694997822,4.77923870217493,333.838939928284));
#57744=CARTESIAN_POINT('Ctrl Pts',(97.3928123900074,4.746835739813,333.705560531681));
#57745=CARTESIAN_POINT('Ctrl Pts',(97.3850552802327,4.70886220233535,333.573609334915));
#57746=CARTESIAN_POINT('Ctrl Pts',(97.377298170458,4.66548249508715,333.443575844914));
#57747=CARTESIAN_POINT('Ctrl Pts',(97.3695369155318,4.62207960711038,333.313472869173));
#57748=CARTESIAN_POINT('Ctrl Pts',(97.3617756606056,4.57326493203777,333.185290007223));
#57749=CARTESIAN_POINT('Ctrl Pts',(97.3540144056795,4.51925107667216,333.059496774417));
#57750=CARTESIAN_POINT('Ctrl Pts',(97.3462407352748,4.46515081674115,332.933502313435));
#57751=CARTESIAN_POINT('Ctrl Pts',(97.3384670648701,4.40583492590786,332.809905472919));
#57752=CARTESIAN_POINT('Ctrl Pts',(97.3306933944655,4.34156242760417,332.689151941448));
#57753=CARTESIAN_POINT('Ctrl Pts',(97.3232815902885,4.28028182956064,332.57401951592));
#57754=CARTESIAN_POINT('Ctrl Pts',(97.3158697861116,4.2144958445608,332.46147189301));
#57755=CARTESIAN_POINT('Ctrl Pts',(97.3084579819346,4.14446458729827,332.351869273029));
#57756=CARTESIAN_POINT('Ctrl Pts',(97.3006829031562,4.07100088950344,332.23689470215));
#57757=CARTESIAN_POINT('Ctrl Pts',(97.2929078243777,3.99263309142799,332.124797779497));
#57758=CARTESIAN_POINT('Ctrl Pts',(97.2851327455993,3.90961342892804,332.016025151104));
#57759=CARTESIAN_POINT('Ctrl Pts',(97.2773672345502,3.82669592740815,331.907386374354));
#57760=CARTESIAN_POINT('Ctrl Pts',(97.2696017235012,3.73913818629106,331.802064060177));
#57761=CARTESIAN_POINT('Ctrl Pts',(97.2618362124522,3.64723691108034,331.700477916887));
#57762=CARTESIAN_POINT('Ctrl Pts',(97.25407840093,3.55542675625205,331.598992496554));
#57763=CARTESIAN_POINT('Ctrl Pts',(97.2463205894079,3.45928189829871,331.501236163089));
#57764=CARTESIAN_POINT('Ctrl Pts',(97.2385627778857,3.35914046444386,331.407597126903));
#57765=CARTESIAN_POINT('Ctrl Pts',(97.2308108043627,3.25907439019338,331.314028557061));
#57766=CARTESIAN_POINT('Ctrl Pts',(97.2230588308397,3.15501801077683,331.22457138318));
#57767=CARTESIAN_POINT('Ctrl Pts',(97.2153068573167,3.04734735468317,331.139578110827));
#57768=CARTESIAN_POINT('Ctrl Pts',(97.2075581667591,2.93972229717629,331.054620833175));
#57769=CARTESIAN_POINT('Ctrl Pts',(97.1998094762015,2.82848631350964,330.974123938731));
#57770=CARTESIAN_POINT('Ctrl Pts',(97.1920607856438,2.71404949390709,330.898400506251));
#57771=CARTESIAN_POINT('Ctrl Pts',(97.184313707266,2.59963648384064,330.822692828663));
#57772=CARTESIAN_POINT('Ctrl Pts',(97.1765666288882,2.48202428824806,330.751756853138));
#57773=CARTESIAN_POINT('Ctrl Pts',(97.1688195505104,2.3616527087174,330.68586282718));
#57774=CARTESIAN_POINT('Ctrl Pts',(97.1610724072045,2.2412801203568,330.619968248967));
#57775=CARTESIAN_POINT('Ctrl Pts',(97.1533252638987,2.11814844479384,330.559115892295));
#57776=CARTESIAN_POINT('Ctrl Pts',(97.1455781205929,1.99272250040752,330.503530262654));
#57777=CARTESIAN_POINT('Ctrl Pts',(97.1378292355648,1.86726835760628,330.447932136183));
#57778=CARTESIAN_POINT('Ctrl Pts',(97.1300803505367,1.7395192768804,330.397603251253));
#57779=CARTESIAN_POINT('Ctrl Pts',(97.1223314655087,1.60996010997533,330.352719988339));
#57780=CARTESIAN_POINT('Ctrl Pts',(97.1145743557339,1.48026342763182,330.307789085865));
#57781=CARTESIAN_POINT('Ctrl Pts',(97.1068172459592,1.34875319116615,330.268315479732));
#57782=CARTESIAN_POINT('Ctrl Pts',(97.0990601361845,1.21593000656208,330.234425818263));
#57783=CARTESIAN_POINT('Ctrl Pts',(97.0912988812583,1.08303584549521,330.200518047242));
#57784=CARTESIAN_POINT('Ctrl Pts',(97.0835376263321,0.948827720553178,330.172200247193));
#57785=CARTESIAN_POINT('Ctrl Pts',(97.075776371406,0.813815510953494,330.14954771422));
#57786=CARTESIAN_POINT('Ctrl Pts',(97.0680027010013,0.678587325818643,330.126858944576));
#57787=CARTESIAN_POINT('Ctrl Pts',(97.0602290305967,0.542552873730515,330.109853600238));
#57788=CARTESIAN_POINT('Ctrl Pts',(97.052455360192,0.406227116165392,330.09855505054));
#57789=CARTESIAN_POINT('Ctrl Pts',(97.0450435560149,0.276247355411802,330.087782451048));
#57790=CARTESIAN_POINT('Ctrl Pts',(97.0376317518377,0.146003086922303,330.082197312579));
#57791=CARTESIAN_POINT('Ctrl Pts',(97.0302199476605,0.0159379738098615,
330.081775824193));
#57792=CARTESIAN_POINT('Ctrl Pts',(97.0224448688821,-0.120502017939399,
330.081333677407));
#57793=CARTESIAN_POINT('Ctrl Pts',(97.0146697901036,-0.257176023963366,
330.086572753744));
#57794=CARTESIAN_POINT('Ctrl Pts',(97.0068947113252,-0.393571950787843,
330.097522648492));
#57795=CARTESIAN_POINT('Ctrl Pts',(96.9991292002761,-0.529800033741066,
330.108459068696));
#57796=CARTESIAN_POINT('Ctrl Pts',(96.9913636892271,-0.665750332466889,
330.12509229357));
#57797=CARTESIAN_POINT('Ctrl Pts',(96.983598178178,-0.800909340915666,330.147399945376));
#57798=CARTESIAN_POINT('Ctrl Pts',(96.9758403666559,-0.935934338813051,
330.169685479081));
#57799=CARTESIAN_POINT('Ctrl Pts',(96.9680825551337,-1.07016922459281,330.19763418));
#57800=CARTESIAN_POINT('Ctrl Pts',(96.9603247436115,-1.20310456379608,330.231171792665));
#57801=CARTESIAN_POINT('Ctrl Pts',(96.9525727700885,-1.33593986494134,330.264684167213));
#57802=CARTESIAN_POINT('Ctrl Pts',(96.9448207965655,-1.46747718859873,330.303776986772));
#57803=CARTESIAN_POINT('Ctrl Pts',(96.9370688230425,-1.59721661472551,330.348324801951));
#57804=CARTESIAN_POINT('Ctrl Pts',(96.9293201324849,-1.72690109612829,330.392853751104));
#57805=CARTESIAN_POINT('Ctrl Pts',(96.9215714419272,-1.85478882547357,330.44283297439));
#57806=CARTESIAN_POINT('Ctrl Pts',(96.9138227513696,-1.98039460480516,330.498087043072));
#57807=CARTESIAN_POINT('Ctrl Pts',(96.9060756729918,-2.10597425080545,330.553329615683));
#57808=CARTESIAN_POINT('Ctrl Pts',(96.898328594614,-2.22927253359901,330.613844693441));
#57809=CARTESIAN_POINT('Ctrl Pts',(96.8905815162361,-2.34982419441821,330.679408684239));
#57810=CARTESIAN_POINT('Ctrl Pts',(96.8828343729303,-2.4703768655766,330.744973224527));
#57811=CARTESIAN_POINT('Ctrl Pts',(96.8750872296244,-2.58818252547101,330.815586575505));
#57812=CARTESIAN_POINT('Ctrl Pts',(96.8673400863186,-2.70280084275048,330.890979354283));
#57813=CARTESIAN_POINT('Ctrl Pts',(96.8595912012905,-2.81744492866101,330.966389082959));
#57814=CARTESIAN_POINT('Ctrl Pts',(96.8518423162624,-2.92889991954033,331.046580162842));
#57815=CARTESIAN_POINT('Ctrl Pts',(96.8440934312342,-3.03675511218316,331.131240321352));
#57816=CARTESIAN_POINT('Ctrl Pts',(96.8363363214595,-3.14472478344174,331.21599033903));
#57817=CARTESIAN_POINT('Ctrl Pts',(96.8285792116848,-3.249086715979,331.305218669248));
#57818=CARTESIAN_POINT('Ctrl Pts',(96.82082210191,-3.34946350189497,331.398572878431));
#57819=CARTESIAN_POINT('Ctrl Pts',(96.8130608469839,-3.44989392595577,331.491976973118));
#57820=CARTESIAN_POINT('Ctrl Pts',(96.8052995920577,-3.5463346854169,331.589511062106));
#57821=CARTESIAN_POINT('Ctrl Pts',(96.7975383371315,-3.63844653727828,331.690787124123));
#57822=CARTESIAN_POINT('Ctrl Pts',(96.7897646667269,-3.73070573808358,331.792225194835));
#57823=CARTESIAN_POINT('Ctrl Pts',(96.7819909963222,-3.81862194261059,331.897416900176));
#57824=CARTESIAN_POINT('Ctrl Pts',(96.7742173259175,-3.90189682388459,332.005941844543));
#57825=CARTESIAN_POINT('Ctrl Pts',(96.7668055217405,-3.98129523939921,332.109414926638));
#57826=CARTESIAN_POINT('Ctrl Pts',(96.7593937175635,-4.05647454858417,332.215917671747));
#57827=CARTESIAN_POINT('Ctrl Pts',(96.7519819133866,-4.1272146829975,332.325064108628));
#57828=CARTESIAN_POINT('Ctrl Pts',(96.7440360237955,-4.20305226373831,332.442075502346));
#57829=CARTESIAN_POINT('Ctrl Pts',(96.7360901342044,-4.27401918672239,332.562482642817));
#57830=CARTESIAN_POINT('Ctrl Pts',(96.7281442446133,-4.33980458986947,332.685852384949));
#57831=CARTESIAN_POINT('Ctrl Pts',(96.7202093851187,-4.40549867292804,332.809050871221));
#57832=CARTESIAN_POINT('Ctrl Pts',(96.7122745256241,-4.46602538477777,332.935203449713));
#57833=CARTESIAN_POINT('Ctrl Pts',(96.7043396661294,-4.52111690709878,333.063847894703));
#57834=CARTESIAN_POINT('Ctrl Pts',(96.6964143958491,-4.57614185175478,333.192336873909));
#57835=CARTESIAN_POINT('Ctrl Pts',(96.6884891255689,-4.62574454215312,333.323311387149));
#57836=CARTESIAN_POINT('Ctrl Pts',(96.6805638552886,-4.6697029614376,333.456284574657));
#57837=CARTESIAN_POINT('Ctrl Pts',(96.6726487998849,-4.71360472273898,333.589086373095));
#57838=CARTESIAN_POINT('Ctrl Pts',(96.6647337444813,-4.75187659762769,333.723881363622));
#57839=CARTESIAN_POINT('Ctrl Pts',(96.6568186890776,-4.78434478643938,333.860163157741));
#57840=CARTESIAN_POINT('Ctrl Pts',(96.6489096294969,-4.81678837990684,333.9963417155));
#57841=CARTESIAN_POINT('Ctrl Pts',(96.6410005699162,-4.84343695578189,334.134004477713));
#57842=CARTESIAN_POINT('Ctrl Pts',(96.6330915103355,-4.86416650873616,334.2726299169));
#57843=CARTESIAN_POINT('Ctrl Pts',(96.6251876881894,-4.88488233443557,334.411163557352));
#57844=CARTESIAN_POINT('Ctrl Pts',(96.6172838660432,-4.89968689245801,334.55065824144));
#57845=CARTESIAN_POINT('Ctrl Pts',(96.6093800438971,-4.90850729581909,334.690582499863));
#57846=CARTESIAN_POINT('Ctrl Pts',(96.6035258214342,-4.91504041391476,334.794221944377));
#57847=CARTESIAN_POINT('Ctrl Pts',(96.5976715989714,-4.91829161310381,334.898096802524));
#57848=CARTESIAN_POINT('Ctrl Pts',(96.5918173765085,-4.91824959781168,335.001989001065));
#57849=CARTESIAN_POINT('',(94.8418173765432,-4.91824873103481,335.0035330121));
#57850=CARTESIAN_POINT('Ctrl Pts',(96.5918173764665,-4.91824959781138,335.001989001811));
#57851=CARTESIAN_POINT('Ctrl Pts',(96.5833945245865,-4.91818914764619,335.151465487433));
#57852=CARTESIAN_POINT('Ctrl Pts',(96.5749716727065,-4.91131016362299,335.300727750483));
#57853=CARTESIAN_POINT('Ctrl Pts',(96.5665488208265,-4.89769596485386,335.449174017898));
#57854=CARTESIAN_POINT('Ctrl Pts',(96.5580887459079,-4.88402160097038,335.598276312655));
#57855=CARTESIAN_POINT('Ctrl Pts',(96.5496286709893,-4.86355244556594,335.746555118912));
#57856=CARTESIAN_POINT('Ctrl Pts',(96.5411685960706,-4.83642350062271,335.893415236676));
#57857=CARTESIAN_POINT('Ctrl Pts',(96.5326895812262,-4.80923382096836,336.040604136368));
#57858=CARTESIAN_POINT('Ctrl Pts',(96.5242105663816,-4.77535461917704,336.186367738042));
#57859=CARTESIAN_POINT('Ctrl Pts',(96.5157315515371,-4.73497092739557,336.330125324629));
#57860=CARTESIAN_POINT('Ctrl Pts',(96.507224131049,-4.69445194575082,336.474364515134));
#57861=CARTESIAN_POINT('Ctrl Pts',(96.4987167105608,-4.64738494710277,336.616583982642));
#57862=CARTESIAN_POINT('Ctrl Pts',(96.4902092900727,-4.59400437601776,336.756219478206));
#57863=CARTESIAN_POINT('Ctrl Pts',(96.4847208197527,-4.55956647789453,336.846303808008));
#57864=CARTESIAN_POINT('Ctrl Pts',(96.4792323494327,-4.52250180143257,336.935313140221));
#57865=CARTESIAN_POINT('Ctrl Pts',(96.4737438791128,-4.4828833428076,337.023101578586));
#57866=CARTESIAN_POINT('Ctrl Pts',(96.4659688003343,-4.42675902784707,337.147464467393));
#57867=CARTESIAN_POINT('Ctrl Pts',(96.4581937215558,-4.36536704404127,337.269686626464));
#57868=CARTESIAN_POINT('Ctrl Pts',(96.4504186427774,-4.29889261447564,337.389289716988));
#57869=CARTESIAN_POINT('Ctrl Pts',(96.4426531317284,-4.23249998592756,337.508745628296));
#57870=CARTESIAN_POINT('Ctrl Pts',(96.4348876206794,-4.16103754390154,337.625588545381));
#57871=CARTESIAN_POINT('Ctrl Pts',(96.4271221096304,-4.08473839951597,337.739360376077));
#57872=CARTESIAN_POINT('Ctrl Pts',(96.4193642981082,-4.00851490595414,337.853019401671));
#57873=CARTESIAN_POINT('Ctrl Pts',(96.4116064865859,-3.92746446986302,337.963613078041));
#57874=CARTESIAN_POINT('Ctrl Pts',(96.4038486750637,-3.84186573159191,338.070708511552));
#57875=CARTESIAN_POINT('Ctrl Pts',(96.3960967015407,-3.75633140908602,338.177723352353));
#57876=CARTESIAN_POINT('Ctrl Pts',(96.3883447280177,-3.66625584025968,338.281244886136));
#57877=CARTESIAN_POINT('Ctrl Pts',(96.3805927544947,-3.57196031738197,338.380870088239));
#57878=CARTESIAN_POINT('Ctrl Pts',(96.3728440639371,-3.47770472871405,338.48045309901));
#57879=CARTESIAN_POINT('Ctrl Pts',(96.3650953733794,-3.3792330086492,338.576142776745));
#57880=CARTESIAN_POINT('Ctrl Pts',(96.3573466828218,-3.27690583841765,338.667570202279));
#57881=CARTESIAN_POINT('Ctrl Pts',(96.349599604444,-3.17459995820858,338.758978605574));
#57882=CARTESIAN_POINT('Ctrl Pts',(96.3418525260661,-3.06844051467748,338.846126260304));
#57883=CARTESIAN_POINT('Ctrl Pts',(96.3341054476883,-2.95882376378397,338.928682348748));
#57884=CARTESIAN_POINT('Ctrl Pts',(96.3263583043825,-2.84920609419659,339.011239129092));
#57885=CARTESIAN_POINT('Ctrl Pts',(96.3186111610767,-2.736131371682,339.089204031244));
#57886=CARTESIAN_POINT('Ctrl Pts',(96.3108640177709,-2.62002720093174,339.162287895963));
#57887=CARTESIAN_POINT('Ctrl Pts',(96.3031151327427,-2.50389692749893,339.235388191485));
#57888=CARTESIAN_POINT('Ctrl Pts',(96.2953662477147,-2.38473618127892,339.303605057765));
#57889=CARTESIAN_POINT('Ctrl Pts',(96.2876173626865,-2.26299932779089,339.366694070452));
#57890=CARTESIAN_POINT('Ctrl Pts',(96.2798602529118,-2.1411332615488,339.429850046469));
#57891=CARTESIAN_POINT('Ctrl Pts',(96.2721031431371,-2.01668597359211,339.487867116342));
#57892=CARTESIAN_POINT('Ctrl Pts',(96.2643460333624,-1.89013458747446,339.540547797759));
#57893=CARTESIAN_POINT('Ctrl Pts',(96.2565847784362,-1.76351557634231,339.593256630048));
#57894=CARTESIAN_POINT('Ctrl Pts',(96.24882352351,-1.63479059329713,339.640623256908));
#57895=CARTESIAN_POINT('Ctrl Pts',(96.2410622685838,-1.50445334011409,339.682499675378));
#57896=CARTESIAN_POINT('Ctrl Pts',(96.2332885981792,-1.37390758980286,339.724443082471));
#57897=CARTESIAN_POINT('Ctrl Pts',(96.2255149277745,-1.24174479254969,339.76087862711));
#57898=CARTESIAN_POINT('Ctrl Pts',(96.2177412573698,-1.10847116395459,339.791708958313));
#57899=CARTESIAN_POINT('Ctrl Pts',(96.2103294531928,-0.981401454835365,
339.821104130181));
#57900=CARTESIAN_POINT('Ctrl Pts',(96.2029176490158,-0.853322288157855,
339.845404136533));
#57901=CARTESIAN_POINT('Ctrl Pts',(96.1955058448387,-0.724676126173611,
339.864568590806));
#57902=CARTESIAN_POINT('Ctrl Pts',(96.1877307660603,-0.589724632572411,
339.88467235207));
#57903=CARTESIAN_POINT('Ctrl Pts',(96.1799556872819,-0.453722686406367,
339.899187946526));
#57904=CARTESIAN_POINT('Ctrl Pts',(96.1721806085035,-0.31717276782418,339.908012275642));
#57905=CARTESIAN_POINT('Ctrl Pts',(96.1644150974544,-0.18079088260991,339.916825745858));
#57906=CARTESIAN_POINT('Ctrl Pts',(96.1566495864054,-0.0438627530047198,
339.919961860654));
#57907=CARTESIAN_POINT('Ctrl Pts',(96.1488840753564,0.0931002517139404,
339.917368748185));
#57908=CARTESIAN_POINT('Ctrl Pts',(96.1411262638342,0.229927457214479,339.914778206795));
#57909=CARTESIAN_POINT('Ctrl Pts',(96.133368452312,0.366789080727974,339.906469750098));
#57910=CARTESIAN_POINT('Ctrl Pts',(96.1256106407898,0.503170304481162,339.892443429125));
#57911=CARTESIAN_POINT('Ctrl Pts',(96.1178586672668,0.639448897038578,339.878427663403));
#57912=CARTESIAN_POINT('Ctrl Pts',(96.1101066937438,0.775247422157984,339.858702637893));
#57913=CARTESIAN_POINT('Ctrl Pts',(96.1023547202208,0.91005309812221,339.833320434349));
#57914=CARTESIAN_POINT('Ctrl Pts',(96.0946060296632,1.04480168380263,339.807948980184));
#57915=CARTESIAN_POINT('Ctrl Pts',(96.0868573391056,1.17855787329232,339.776925185274));
#57916=CARTESIAN_POINT('Ctrl Pts',(96.079108648548,1.31081624928653,339.740352710833));
#57917=CARTESIAN_POINT('Ctrl Pts',(96.0713615701702,1.44304710782097,339.703787845601));
#57918=CARTESIAN_POINT('Ctrl Pts',(96.0636144917924,1.57378039621972,339.66167670123));
#57919=CARTESIAN_POINT('Ctrl Pts',(96.0558674134145,1.70252348596556,339.614173473357));
#57920=CARTESIAN_POINT('Ctrl Pts',(96.0481202701087,1.83126765470251,339.566669847362));
#57921=CARTESIAN_POINT('Ctrl Pts',(96.0403731268029,1.95802122480944,339.513774183036));
#57922=CARTESIAN_POINT('Ctrl Pts',(96.0326259834971,2.08230963467583,339.455689581629));
#57923=CARTESIAN_POINT('Ctrl Pts',(96.024877098469,2.20662598721531,339.39759192157));
#57924=CARTESIAN_POINT('Ctrl Pts',(96.0171282134409,2.32847572263421,339.334303168518));
#57925=CARTESIAN_POINT('Ctrl Pts',(96.0093793284129,2.44740741602913,339.26607313609));
#57926=CARTESIAN_POINT('Ctrl Pts',(96.0016222186381,2.56646534475237,339.1977706836));
#57927=CARTESIAN_POINT('Ctrl Pts',(95.9938651088634,2.68259870484572,339.124516669718));
#57928=CARTESIAN_POINT('Ctrl Pts',(95.9861079990887,2.79538323028787,339.046605448808));
#57929=CARTESIAN_POINT('Ctrl Pts',(95.9783467441626,2.90822802417418,338.968652594633));
#57930=CARTESIAN_POINT('Ctrl Pts',(95.9705854892364,3.01772010578734,338.886037809854));
#57931=CARTESIAN_POINT('Ctrl Pts',(95.9628242343102,3.12346784592035,338.799096165932));
#57932=CARTESIAN_POINT('Ctrl Pts',(95.9550505639056,3.22938474797446,338.712015443714));
#57933=CARTESIAN_POINT('Ctrl Pts',(95.9472768935009,3.33154504787365,338.62059429181));
#57934=CARTESIAN_POINT('Ctrl Pts',(95.9395032230963,3.42959293879054,338.525205715515));
#57935=CARTESIAN_POINT('Ctrl Pts',(95.9320914189191,3.52307667679721,338.434257500394));
#57936=CARTESIAN_POINT('Ctrl Pts',(95.924679614742,3.6128220568282,338.339703124455));
#57937=CARTESIAN_POINT('Ctrl Pts',(95.9172678105648,3.69855567524792,338.241892808159));
#57938=CARTESIAN_POINT('Ctrl Pts',(95.9094927317864,3.78849135369295,338.139288516899));
#57939=CARTESIAN_POINT('Ctrl Pts',(95.9017176530079,3.87429628360831,338.032776799959));
#57940=CARTESIAN_POINT('Ctrl Pts',(95.8939425742295,3.95561184639788,337.922724411082));
#57941=CARTESIAN_POINT('Ctrl Pts',(95.8861770631805,4.03682734521063,337.812807448677));
#57942=CARTESIAN_POINT('Ctrl Pts',(95.8784115521315,4.11356423891229,337.699358794924));
#57943=CARTESIAN_POINT('Ctrl Pts',(95.8706460410825,4.18550217610446,337.582780400329));
#57944=CARTESIAN_POINT('Ctrl Pts',(95.8628882295603,4.25736878662246,337.466317593552));
#57945=CARTESIAN_POINT('Ctrl Pts',(95.8551304180381,4.3244457057346,337.346731551867));
#57946=CARTESIAN_POINT('Ctrl Pts',(95.8473726065159,4.38645437891549,337.224455224138));
#57947=CARTESIAN_POINT('Ctrl Pts',(95.8396206329929,4.4484163886034,337.102270913223));
#57948=CARTESIAN_POINT('Ctrl Pts',(95.8318686594699,4.50531756789691,336.97740069319));
#57949=CARTESIAN_POINT('Ctrl Pts',(95.8241166859468,4.55692421784395,336.850303957551));
#57950=CARTESIAN_POINT('Ctrl Pts',(95.8163679953892,4.60850901234409,336.723261047454));
#57951=CARTESIAN_POINT('Ctrl Pts',(95.8086193048316,4.65480359040232,336.593993858578));
#57952=CARTESIAN_POINT('Ctrl Pts',(95.800870614274,4.69562161263999,336.462983504148));
#57953=CARTESIAN_POINT('Ctrl Pts',(95.7931235358961,4.73643114234722,336.332000407516));
#57954=CARTESIAN_POINT('Ctrl Pts',(95.7853764575183,4.77176626647043,336.199275239672));
#57955=CARTESIAN_POINT('Ctrl Pts',(95.7776293791405,4.80149006185392,336.065305706555));
#57956=CARTESIAN_POINT('Ctrl Pts',(95.7698822358347,4.83121410635141,335.931335050644));
#57957=CARTESIAN_POINT('Ctrl Pts',(95.7621350925289,4.85532664364326,335.796120390252));
#57958=CARTESIAN_POINT('Ctrl Pts',(95.754387949223,4.87374165338536,335.660170704104));
#57959=CARTESIAN_POINT('Ctrl Pts',(95.7466390641949,4.89216080321262,335.524190453579));
#57960=CARTESIAN_POINT('Ctrl Pts',(95.7388901791668,4.90487982413585,335.38747523573));
#57961=CARTESIAN_POINT('Ctrl Pts',(95.7311412941387,4.91186449783825,335.250539851872));
#57962=CARTESIAN_POINT('Ctrl Pts',(95.723384184364,4.91885658514548,335.113459123383));
#57963=CARTESIAN_POINT('Ctrl Pts',(95.7156270745892,4.92010214694343,334.976158153058));
#57964=CARTESIAN_POINT('Ctrl Pts',(95.7078699648145,4.91561911740867,334.839153007282));
#57965=CARTESIAN_POINT('Ctrl Pts',(95.7001087098884,4.91113369228627,334.702074650337));
#57966=CARTESIAN_POINT('Ctrl Pts',(95.6923474549622,4.90091360527163,334.565292822518));
#57967=CARTESIAN_POINT('Ctrl Pts',(95.684586200036,4.88502869206876,334.429318179574));
#57968=CARTESIAN_POINT('Ctrl Pts',(95.6768125296313,4.86911836818165,334.293126021515));
#57969=CARTESIAN_POINT('Ctrl Pts',(95.6690388592267,4.84752517139296,334.157744014796));
#57970=CARTESIAN_POINT('Ctrl Pts',(95.661265188822,4.8203702223217,334.023673219534));
#57971=CARTESIAN_POINT('Ctrl Pts',(95.653853384645,4.79447934266315,333.89584345205));
#57972=CARTESIAN_POINT('Ctrl Pts',(95.646441580468,4.76353292543133,333.769205849001));
#57973=CARTESIAN_POINT('Ctrl Pts',(95.639029776291,4.72767752408759,333.644179845725));
#57974=CARTESIAN_POINT('Ctrl Pts',(95.6312546975126,4.6900647427158,333.513025945594));
#57975=CARTESIAN_POINT('Ctrl Pts',(95.6234796187342,4.64693073867575,333.383231147783));
#57976=CARTESIAN_POINT('Ctrl Pts',(95.6157045399557,4.59838985391638,333.255295493816));
#57977=CARTESIAN_POINT('Ctrl Pts',(95.6079390289067,4.54990870180596,333.127517272816));
#57978=CARTESIAN_POINT('Ctrl Pts',(95.6001735178577,4.4960340448888,333.001594005565));
#57979=CARTESIAN_POINT('Ctrl Pts',(95.5924080068087,4.43693053139547,332.878012600869));
#57980=CARTESIAN_POINT('Ctrl Pts',(95.5846501952865,4.37788561920789,332.754553727496));
#57981=CARTESIAN_POINT('Ctrl Pts',(95.5768923837643,4.31362233530307,332.63343244619));
#57982=CARTESIAN_POINT('Ctrl Pts',(95.5691345722421,4.24435401377999,332.515117292867));
#57983=CARTESIAN_POINT('Ctrl Pts',(95.5613825987191,4.17513781886548,332.396891175449));
#57984=CARTESIAN_POINT('Ctrl Pts',(95.5536306251961,4.1009242799554,332.281467318736));
#57985=CARTESIAN_POINT('Ctrl Pts',(95.5458786516731,4.0219732429417,332.169290849352));
#57986=CARTESIAN_POINT('Ctrl Pts',(95.5381299611155,3.94305564173905,332.05716188677));
#57987=CARTESIAN_POINT('Ctrl Pts',(95.5303812705579,3.8594047573886,331.948277895179));
#57988=CARTESIAN_POINT('Ctrl Pts',(95.5226325800003,3.77132432933522,331.84305592931));
#57989=CARTESIAN_POINT('Ctrl Pts',(95.5148855016224,3.68326222715057,331.73785585575));
#57990=CARTESIAN_POINT('Ctrl Pts',(95.5071384232446,3.59077266513595,331.636316591944));
#57991=CARTESIAN_POINT('Ctrl Pts',(95.4993913448668,3.49420007785615,331.538822616737));
#57992=CARTESIAN_POINT('Ctrl Pts',(95.4916442015609,3.39762668120513,331.441327824437));
#57993=CARTESIAN_POINT('Ctrl Pts',(95.4838970582552,3.29697046610974,331.347878666056));
#57994=CARTESIAN_POINT('Ctrl Pts',(95.4761499149494,3.19261289309245,331.25882291553));
#57995=CARTESIAN_POINT('Ctrl Pts',(95.4684010299213,3.08823185827717,331.169747143381));
#57996=CARTESIAN_POINT('Ctrl Pts',(95.4606521448932,2.98014810693591,331.085066998243));
#57997=CARTESIAN_POINT('Ctrl Pts',(95.4529032598651,2.86877602898271,331.005089843559));
#57998=CARTESIAN_POINT('Ctrl Pts',(95.4451461500904,2.75728573955521,330.925027800297));
#57999=CARTESIAN_POINT('Ctrl Pts',(95.4373890403156,2.64250046938033,330.849678947437));
#58000=CARTESIAN_POINT('Ctrl Pts',(95.4296319305409,2.52486389490342,330.779307476881));
#58001=CARTESIAN_POINT('Ctrl Pts',(95.4218706756147,2.40716445920239,330.708898402061));
#58002=CARTESIAN_POINT('Ctrl Pts',(95.4141094206885,2.28661102656509,330.643472195695));
#58003=CARTESIAN_POINT('Ctrl Pts',(95.4063481657624,2.16367081041174,330.583246476577));
#58004=CARTESIAN_POINT('Ctrl Pts',(95.3985744953577,2.04053392997867,330.522924415935));
#58005=CARTESIAN_POINT('Ctrl Pts',(95.3908008249531,1.91500299448009,330.467819623731));
#58006=CARTESIAN_POINT('Ctrl Pts',(95.3830271545484,1.78756490137708,330.418101399434));
#58007=CARTESIAN_POINT('Ctrl Pts',(95.3756153503712,1.66605908216638,330.370697570439));
#58008=CARTESIAN_POINT('Ctrl Pts',(95.3682035461941,1.54281993799597,330.328190199428));
#58009=CARTESIAN_POINT('Ctrl Pts',(95.3607917420169,1.41827948947577,330.290683026995));
#58010=CARTESIAN_POINT('Ctrl Pts',(95.3530166632384,1.28763494258823,330.251337516314));
#58011=CARTESIAN_POINT('Ctrl Pts',(95.34524158446,1.1551454434434,330.217370407815));
#58012=CARTESIAN_POINT('Ctrl Pts',(95.3374665056816,1.0212933646164,330.188956150076));
#58013=CARTESIAN_POINT('Ctrl Pts',(95.3297009946325,0.887605999293833,330.16057685789));
#58014=CARTESIAN_POINT('Ctrl Pts',(95.3219354835835,0.752559769222005,330.137736900872));
#58015=CARTESIAN_POINT('Ctrl Pts',(95.3141699725345,0.616653227009483,330.120561317106));
#58016=CARTESIAN_POINT('Ctrl Pts',(95.3064121610123,0.480881436529245,330.103402762982));
#58017=CARTESIAN_POINT('Ctrl Pts',(95.2986543494901,0.344251416722254,330.091897454162));
#58018=CARTESIAN_POINT('Ctrl Pts',(95.2908965379679,0.207272616758024,330.086119545121));
#58019=CARTESIAN_POINT('Ctrl Pts',(95.2831445644449,0.0703968976847071,
330.080345984139));
#58020=CARTESIAN_POINT('Ctrl Pts',(95.2753925909219,-0.0668266901612984,
330.080291260399));
#58021=CARTESIAN_POINT('Ctrl Pts',(95.2676406173989,-0.203883212783746,
330.085977747502));
#58022=CARTESIAN_POINT('Ctrl Pts',(95.2598919268413,-0.340881691887493,
330.091661826375));
#58023=CARTESIAN_POINT('Ctrl Pts',(95.2521432362837,-0.477712856763349,
330.103082264027));
#58024=CARTESIAN_POINT('Ctrl Pts',(95.2443945457261,-0.613861626348289,
330.120209331724));
#58025=CARTESIAN_POINT('Ctrl Pts',(95.2366474673482,-0.74998206904458,330.137332835991));
#58026=CARTESIAN_POINT('Ctrl Pts',(95.2289003889704,-0.885420011280039,
330.160160559901));
#58027=CARTESIAN_POINT('Ctrl Pts',(95.2211533105925,-1.01966574328563,330.188610924642));
#58028=CARTESIAN_POINT('Ctrl Pts',(95.2134061672867,-1.15391260039966,330.217061527826));
#58029=CARTESIAN_POINT('Ctrl Pts',(95.2056590239809,-1.28696684497268,330.251134784794));
#58030=CARTESIAN_POINT('Ctrl Pts',(95.1979118806751,-1.4183295963068,330.290698117689));
#58031=CARTESIAN_POINT('Ctrl Pts',(95.1901629956471,-1.54972188077615,330.33027034526));
#58032=CARTESIAN_POINT('Ctrl Pts',(95.182414110619,-1.67942154108957,330.375334992149));
#58033=CARTESIAN_POINT('Ctrl Pts',(95.1746652255909,-1.80694585860989,330.425709921031));
#58034=CARTESIAN_POINT('Ctrl Pts',(95.1669081158161,-1.93460553175857,330.476138318384));
#58035=CARTESIAN_POINT('Ctrl Pts',(95.1591510060414,-2.0600848856947,330.531888113111));
#58036=CARTESIAN_POINT('Ctrl Pts',(95.1513938962667,-2.1829216570294,330.592729177623));
#58037=CARTESIAN_POINT('Ctrl Pts',(95.1436326413405,-2.30582406840723,330.653602753655));
#58038=CARTESIAN_POINT('Ctrl Pts',(95.1358713864144,-2.42608074090186,330.719572832635));
#58039=CARTESIAN_POINT('Ctrl Pts',(95.1281101314882,-2.54325583823656,330.790364290847));
#58040=CARTESIAN_POINT('Ctrl Pts',(95.1203364610835,-2.66061837753965,330.861268992321));
#58041=CARTESIAN_POINT('Ctrl Pts',(95.1125627906789,-2.77488916507475,330.937010269093));
#58042=CARTESIAN_POINT('Ctrl Pts',(95.1047891202742,-2.88566234515216,331.017270296358));
#58043=CARTESIAN_POINT('Ctrl Pts',(95.0973773160972,-2.99127900704595,331.093794200044));
#58044=CARTESIAN_POINT('Ctrl Pts',(95.0899655119201,-3.09371613455408,331.17442544804));
#58045=CARTESIAN_POINT('Ctrl Pts',(95.0825537077431,-3.19265269885515,331.258856884989));
#58046=CARTESIAN_POINT('Ctrl Pts',(95.0748901037727,-3.29495041596678,331.346156694856));
#58047=CARTESIAN_POINT('Ctrl Pts',(95.0672264998024,-3.39384881934144,331.437812771077));
#58048=CARTESIAN_POINT('Ctrl Pts',(95.059562895832,-3.48894604651845,331.533526497003));
#58049=CARTESIAN_POINT('Ctrl Pts',(95.0519087841593,-3.58392548431247,331.629121669937));
#58050=CARTESIAN_POINT('Ctrl Pts',(95.0442546724865,-3.67511282771166,331.728764214921));
#58051=CARTESIAN_POINT('Ctrl Pts',(95.0366005608138,-3.7621384884469,331.832114734362));
#58052=CARTESIAN_POINT('Ctrl Pts',(95.0289539735891,-3.8490785977698,331.935363654082));
#58053=CARTESIAN_POINT('Ctrl Pts',(95.0213073863645,-3.93186490413887,332.042312991526));
#58054=CARTESIAN_POINT('Ctrl Pts',(95.0136607991398,-4.01016435594877,332.152586278607));
#58055=CARTESIAN_POINT('Ctrl Pts',(95.0060199106811,-4.08840545358838,332.262777382403));
#58056=CARTESIAN_POINT('Ctrl Pts',(94.9983790222224,-4.16216611803201,332.376287179157));
#58057=CARTESIAN_POINT('Ctrl Pts',(94.9907381337637,-4.23115367591782,332.492706312921));
#58058=CARTESIAN_POINT('Ctrl Pts',(94.9831002448847,-4.30011415139341,332.609079744085));
#58059=CARTESIAN_POINT('Ctrl Pts',(94.9754623560057,-4.36430504078019,332.728359895267));
#58060=CARTESIAN_POINT('Ctrl Pts',(94.9678244671267,-4.42347731560101,332.850108956048));
#58061=CARTESIAN_POINT('Ctrl Pts',(94.9601878128149,-4.48264002597855,332.971838337647));
#58062=CARTESIAN_POINT('Ctrl Pts',(94.9525511585032,-4.53678555946599,333.096035472577));
#58063=CARTESIAN_POINT('Ctrl Pts',(94.9449145041915,-4.58571139008812,333.222239017945));
#58064=CARTESIAN_POINT('Ctrl Pts',(94.9372773207062,-4.63464061097224,333.348451308451));
#58065=CARTESIAN_POINT('Ctrl Pts',(94.9296401372208,-4.67834926551093,333.476669909567));
#58066=CARTESIAN_POINT('Ctrl Pts',(94.9220029537354,-4.7166836177908,333.606415157888));
#58067=CARTESIAN_POINT('Ctrl Pts',(94.914359929218,-4.75504728875635,333.736259637315));
#58068=CARTESIAN_POINT('Ctrl Pts',(94.9067169047005,-4.78802833608416,333.867632708348));
#58069=CARTESIAN_POINT('Ctrl Pts',(94.8990738801831,-4.81552337000894,334.000041133147));
#58070=CARTESIAN_POINT('Ctrl Pts',(94.891427580026,-4.84303018772731,334.132506305414));
#58071=CARTESIAN_POINT('Ctrl Pts',(94.8837812798689,-4.86504624396026,334.266007317853));
#58072=CARTESIAN_POINT('Ctrl Pts',(94.8761349797118,-4.88151980372615,334.400043777989));
#58073=CARTESIAN_POINT('Ctrl Pts',(94.8684794165725,-4.89801332011002,334.53424261435));
#58074=CARTESIAN_POINT('Ctrl Pts',(94.8608238534331,-4.90895090241172,334.668977792443));
#58075=CARTESIAN_POINT('Ctrl Pts',(94.8531682902938,-4.9143328816872,334.803746616671));
#58076=CARTESIAN_POINT('Ctrl Pts',(94.849384652377,-4.91699283765438,334.870353922246));
#58077=CARTESIAN_POINT('Ctrl Pts',(94.8456010144601,-4.91829654678943,334.936969477117));
#58078=CARTESIAN_POINT('Ctrl Pts',(94.8418173765432,-4.91824873103481,335.0035330121));
#58079=CARTESIAN_POINT('',(93.0918173764785,-4.91824847853219,334.996131419409));
#58080=CARTESIAN_POINT('Ctrl Pts',(94.8418173765085,-4.91824873103437,335.00353301271));
#58081=CARTESIAN_POINT('Ctrl Pts',(94.8293168088287,-4.91809075498242,335.223448869443));
#58082=CARTESIAN_POINT('Ctrl Pts',(94.8168162411489,-4.90318214465297,335.442842262135));
#58083=CARTESIAN_POINT('Ctrl Pts',(94.8043156734691,-4.87373462892463,335.660222560445));
#58084=CARTESIAN_POINT('Ctrl Pts',(94.7965405946907,-4.85541892035186,335.795428335698));
#58085=CARTESIAN_POINT('Ctrl Pts',(94.7887655159123,-4.83144374547594,335.930085020765));
#58086=CARTESIAN_POINT('Ctrl Pts',(94.7809904371338,-4.80185017708903,336.063681314723));
#58087=CARTESIAN_POINT('Ctrl Pts',(94.7732249260848,-4.77229302547203,336.197113209936));
#58088=CARTESIAN_POINT('Ctrl Pts',(94.7654594150358,-4.73713132053269,336.3294869324));
#58089=CARTESIAN_POINT('Ctrl Pts',(94.7576939039868,-4.69645780895182,336.460296925709));
#58090=CARTESIAN_POINT('Ctrl Pts',(94.7499360924646,-4.6558246252761,336.590977220529));
#58091=CARTESIAN_POINT('Ctrl Pts',(94.7421782809424,-4.6096906258712,336.720096500818));
#58092=CARTESIAN_POINT('Ctrl Pts',(94.7344204694202,-4.55819938312424,336.847160373705));
#58093=CARTESIAN_POINT('Ctrl Pts',(94.7266684958972,-4.50674688917036,336.974128626998));
#58094=CARTESIAN_POINT('Ctrl Pts',(94.7189165223742,-4.44994532257975,337.099044190835));
#58095=CARTESIAN_POINT('Ctrl Pts',(94.7111645488512,-4.38798765601154,337.221429133056));
#58096=CARTESIAN_POINT('Ctrl Pts',(94.7034158582935,-4.32605622855186,337.343762245181));
#58097=CARTESIAN_POINT('Ctrl Pts',(94.6956671677359,-4.25897322034282,337.463566519258));
#58098=CARTESIAN_POINT('Ctrl Pts',(94.6879184771782,-4.18697908547576,337.580385475135));
#58099=CARTESIAN_POINT('Ctrl Pts',(94.6801713988004,-4.11499992958977,337.697180125853));
#58100=CARTESIAN_POINT('Ctrl Pts',(94.6724243204226,-4.03811188442553,337.810990361274));
#58101=CARTESIAN_POINT('Ctrl Pts',(94.6646772420447,-3.95660036967125,337.921386071237));
#58102=CARTESIAN_POINT('Ctrl Pts',(94.6569300987389,-3.87508817177203,338.031782706422));
#58103=CARTESIAN_POINT('Ctrl Pts',(94.6491829554331,-3.78895265916973,338.138764444621));
#58104=CARTESIAN_POINT('Ctrl Pts',(94.6414358121273,-3.69852118145261,338.241932160432));
#58105=CARTESIAN_POINT('Ctrl Pts',(94.6336869270992,-3.60806937281932,338.345123070537));
#58106=CARTESIAN_POINT('Ctrl Pts',(94.6259380420711,-3.51331993478883,338.444497958097));
#58107=CARTESIAN_POINT('Ctrl Pts',(94.618189157043,-3.41463862717781,338.53969293983));
#58108=CARTESIAN_POINT('Ctrl Pts',(94.6104320472682,-3.31585257820739,338.634988962501));
#58109=CARTESIAN_POINT('Ctrl Pts',(94.6026749374935,-3.21312660480307,338.726095945025));
#58110=CARTESIAN_POINT('Ctrl Pts',(94.5949178277188,-3.10686167016336,338.812688503533));
#58111=CARTESIAN_POINT('Ctrl Pts',(94.5871565727926,-3.00053995094027,338.899327334335));
#58112=CARTESIAN_POINT('Ctrl Pts',(94.5793953178664,-2.89067581520077,338.981446700372));
#58113=CARTESIAN_POINT('Ctrl Pts',(94.5716340629402,-2.77770023030416,339.058763911965));
#58114=CARTESIAN_POINT('Ctrl Pts',(94.5638603925356,-2.66454392129045,339.136204805898));
#58115=CARTESIAN_POINT('Ctrl Pts',(94.5560867221309,-2.54826654869037,339.208827987543));
#58116=CARTESIAN_POINT('Ctrl Pts',(94.5483130517262,-2.42932552302091,339.276395744748));
#58117=CARTESIAN_POINT('Ctrl Pts',(94.5409012475492,-2.31592123071321,339.340818206598));
#58118=CARTESIAN_POINT('Ctrl Pts',(94.5334894433722,-2.20009594636449,339.400645180038));
#58119=CARTESIAN_POINT('Ctrl Pts',(94.5260776391952,-2.08226222623539,339.455711737051));
#58120=CARTESIAN_POINT('Ctrl Pts',(94.5183025604168,-1.95865312447281,339.513477270059));
#58121=CARTESIAN_POINT('Ctrl Pts',(94.5105274816384,-1.83244310240549,339.566186492906));
#58122=CARTESIAN_POINT('Ctrl Pts',(94.5027524028599,-1.70408435073156,339.613597250313));
#58123=CARTESIAN_POINT('Ctrl Pts',(94.4949868918109,-1.57588355267328,339.660949665764));
#58124=CARTESIAN_POINT('Ctrl Pts',(94.4872213807619,-1.44553964926298,339.703016454766));
#58125=CARTESIAN_POINT('Ctrl Pts',(94.4794558697129,-1.31352796421854,339.739602024402));
#58126=CARTESIAN_POINT('Ctrl Pts',(94.4716980581907,-1.18164716914417,339.776151319339));
#58127=CARTESIAN_POINT('Ctrl Pts',(94.4639402466685,-1.04810225746365,339.807230106441));
#58128=CARTESIAN_POINT('Ctrl Pts',(94.4561824351463,-0.913386669947358,
339.83269157444));
#58129=CARTESIAN_POINT('Ctrl Pts',(94.4484304616233,-0.778772460182841,
339.858133881877));
#58130=CARTESIAN_POINT('Ctrl Pts',(94.4406784881003,-0.642989710639765,
339.877967211969));
#58131=CARTESIAN_POINT('Ctrl Pts',(94.4329265145773,-0.50654475324799,339.892095203025));
#58132=CARTESIAN_POINT('Ctrl Pts',(94.4251778240196,-0.370157580376678,
339.906217210868));
#58133=CARTESIAN_POINT('Ctrl Pts',(94.417429133462,-0.233109145429348,339.914638645183));
#58134=CARTESIAN_POINT('Ctrl Pts',(94.4096804429044,-0.0959134358103597,
339.917314681341));
#58135=CARTESIAN_POINT('Ctrl Pts',(94.4019333645266,0.0412537290953617,
339.919990160727));
#58136=CARTESIAN_POINT('Ctrl Pts',(94.3941862861487,0.178567717169585,339.916922612031));
#58137=CARTESIAN_POINT('Ctrl Pts',(94.3864392077709,0.315512382629436,339.908119293467));
#58138=CARTESIAN_POINT('Ctrl Pts',(94.3786920644651,0.452458195817486,339.899315901124));
#58139=CARTESIAN_POINT('Ctrl Pts',(94.3709449211593,0.589034290148235,339.884776668106));
#58140=CARTESIAN_POINT('Ctrl Pts',(94.3631977778535,0.724727884910329,339.864560880011));
#58141=CARTESIAN_POINT('Ctrl Pts',(94.3554488928254,0.860451986473198,339.844340546977));
#58142=CARTESIAN_POINT('Ctrl Pts',(94.3477000077973,0.995292807132512,339.818441176936));
#58143=CARTESIAN_POINT('Ctrl Pts',(94.3399511227692,1.12874641604819,339.786973426995));
#58144=CARTESIAN_POINT('Ctrl Pts',(94.3321940129945,1.26234167400339,339.75547227686));
#58145=CARTESIAN_POINT('Ctrl Pts',(94.3244369032197,1.39454639791398,339.718391030223));
#58146=CARTESIAN_POINT('Ctrl Pts',(94.316679793445,1.52486998134862,339.67589078171));
#58147=CARTESIAN_POINT('Ctrl Pts',(94.3089185385189,1.65526320553931,339.633367822424));
#58148=CARTESIAN_POINT('Ctrl Pts',(94.3011572835927,1.78377292023109,339.585420227803));
#58149=CARTESIAN_POINT('Ctrl Pts',(94.2933960286665,1.90992818447491,339.532257427888));
#58150=CARTESIAN_POINT('Ctrl Pts',(94.2856223582618,2.03628525602753,339.47900958482));
#58151=CARTESIAN_POINT('Ctrl Pts',(94.2778486878572,2.16027999712832,339.420530032237));
#58152=CARTESIAN_POINT('Ctrl Pts',(94.2700750174526,2.28146497948108,339.357074776717));
#58153=CARTESIAN_POINT('Ctrl Pts',(94.2626632132755,2.39700877174998,339.296573378607));
#58154=CARTESIAN_POINT('Ctrl Pts',(94.2552514090984,2.50999825748356,339.231549234173));
#58155=CARTESIAN_POINT('Ctrl Pts',(94.2478396049213,2.62007148732974,339.162260018762));
#58156=CARTESIAN_POINT('Ctrl Pts',(94.2400645261428,2.73553973406183,339.089574732501));
#58157=CARTESIAN_POINT('Ctrl Pts',(94.2322894473644,2.84816352892613,339.011966017309));
#58158=CARTESIAN_POINT('Ctrl Pts',(94.224514368586,2.95749453204789,338.929683085874));
#58159=CARTESIAN_POINT('Ctrl Pts',(94.216748857537,3.06669099641003,338.847501408825));
#58160=CARTESIAN_POINT('Ctrl Pts',(94.2089833464879,3.17260242200452,338.760657193003));
#58161=CARTESIAN_POINT('Ctrl Pts',(94.2012178354389,3.27480710563654,338.669444301713));
#58162=CARTESIAN_POINT('Ctrl Pts',(94.1934600239167,3.3769104530271,338.57832184827));
#58163=CARTESIAN_POINT('Ctrl Pts',(94.1857022123945,3.47531408265366,338.482839597984));
#58164=CARTESIAN_POINT('Ctrl Pts',(94.1779444008723,3.56962750867437,338.383333047723));
#58165=CARTESIAN_POINT('Ctrl Pts',(94.1701924273493,3.66386996085115,338.283901379297));
#58166=CARTESIAN_POINT('Ctrl Pts',(94.1624404538264,3.75402806824117,338.180451721358));
#58167=CARTESIAN_POINT('Ctrl Pts',(94.1546884803033,3.83974679298242,338.073357712386));
#58168=CARTESIAN_POINT('Ctrl Pts',(94.1469397897457,3.92542921579286,337.96630905779));
#58169=CARTESIAN_POINT('Ctrl Pts',(94.1391910991881,4.00667575155903,337.855619426373));
#58170=CARTESIAN_POINT('Ctrl Pts',(94.1314424086305,4.08317055821811,337.741696783928));
#58171=CARTESIAN_POINT('Ctrl Pts',(94.1236953302526,4.15964944949376,337.627797844041));
#58172=CARTESIAN_POINT('Ctrl Pts',(94.1159482518748,4.23137836037357,337.510667555388));
#58173=CARTESIAN_POINT('Ctrl Pts',(94.108201173497,4.29808407834662,337.390743883808));
#58174=CARTESIAN_POINT('Ctrl Pts',(94.1004540301912,4.3647903553778,337.270819207151));
#58175=CARTESIAN_POINT('Ctrl Pts',(94.0927068868854,4.42647316552963,337.148101442459));
#58176=CARTESIAN_POINT('Ctrl Pts',(94.0849597435796,4.48290486825782,337.023053880808));
#58177=CARTESIAN_POINT('Ctrl Pts',(94.0772108585515,4.53934925803082,336.89797820581));
#58178=CARTESIAN_POINT('Ctrl Pts',(94.0694619735234,4.59054003044752,336.770572047779));
#58179=CARTESIAN_POINT('Ctrl Pts',(94.0617130884953,4.63629753353837,336.641319055822));
#58180=CARTESIAN_POINT('Ctrl Pts',(94.0539559787206,4.6821036041158,336.511928873404));
#58181=CARTESIAN_POINT('Ctrl Pts',(94.0461988689459,4.72246475473862,336.380688310327));
#58182=CARTESIAN_POINT('Ctrl Pts',(94.0384417591711,4.75725095802335,336.248097105551));
#58183=CARTESIAN_POINT('Ctrl Pts',(94.030680504245,4.79205574994286,336.115435048275));
#58184=CARTESIAN_POINT('Ctrl Pts',(94.0229192493188,4.82127957521477,335.981421292875));
#58185=CARTESIAN_POINT('Ctrl Pts',(94.0151579943927,4.84484369485811,335.846565198253));
#58186=CARTESIAN_POINT('Ctrl Pts',(94.007384323988,4.86844550941335,335.71149337783));
#58187=CARTESIAN_POINT('Ctrl Pts',(93.9996106535833,4.88636947526628,335.575576913268));
#58188=CARTESIAN_POINT('Ctrl Pts',(93.9918369831787,4.89858874468487,335.439330596415));
#58189=CARTESIAN_POINT('Ctrl Pts',(93.9844251790016,4.91023920417228,335.309426578391));
#58190=CARTESIAN_POINT('Ctrl Pts',(93.9770133748245,4.9167041079539,335.179223013674));
#58191=CARTESIAN_POINT('Ctrl Pts',(93.9696015706473,4.91800426916427,335.049163716113));
#58192=CARTESIAN_POINT('Ctrl Pts',(93.9618264918689,4.91936815514853,334.912729824952));
#58193=CARTESIAN_POINT('Ctrl Pts',(93.9540514130905,4.91505252858747,334.77602354415));
#58194=CARTESIAN_POINT('Ctrl Pts',(93.946276334312,4.90502433531529,334.639556755557));
#58195=CARTESIAN_POINT('Ctrl Pts',(93.938510823263,4.89500848237336,334.503257898035));
#58196=CARTESIAN_POINT('Ctrl Pts',(93.930745312214,4.87929407813407,334.36719833243));
#58197=CARTESIAN_POINT('Ctrl Pts',(93.922979801165,4.8579000307232,334.23189170425));
#58198=CARTESIAN_POINT('Ctrl Pts',(93.9152219896427,4.83652719557265,334.096719232987));
#58199=CARTESIAN_POINT('Ctrl Pts',(93.9074641781205,4.80948598467219,333.962298597084));
#58200=CARTESIAN_POINT('Ctrl Pts',(93.8997063665983,4.77684721020204,333.829139721023));
#58201=CARTESIAN_POINT('Ctrl Pts',(93.8919543930753,4.74423299744472,333.69608105124));
#58202=CARTESIAN_POINT('Ctrl Pts',(93.8842024195523,4.70602969826126,333.564282629445));
#58203=CARTESIAN_POINT('Ctrl Pts',(93.8764504460292,4.66235938186314,333.434245211774));
#58204=CARTESIAN_POINT('Ctrl Pts',(93.8687017554716,4.61870755986995,333.304262865026));
#58205=CARTESIAN_POINT('Ctrl Pts',(93.860953064914,4.56959344977913,333.176040408851));
#58206=CARTESIAN_POINT('Ctrl Pts',(93.8532043743564,4.51518919846861,333.05006421528));
#58207=CARTESIAN_POINT('Ctrl Pts',(93.8454572959785,4.46079626641697,332.924114232108));
#58208=CARTESIAN_POINT('Ctrl Pts',(93.8377102176007,4.40111553730479,332.800409940555));
#58209=CARTESIAN_POINT('Ctrl Pts',(93.8299631392229,4.33636745498178,332.679418099296));
#58210=CARTESIAN_POINT('Ctrl Pts',(93.822215995917,4.27161883000751,332.558425244009));
#58211=CARTESIAN_POINT('Ctrl Pts',(93.8144688526112,4.20180295154076,332.440145228988));
#58212=CARTESIAN_POINT('Ctrl Pts',(93.8067217093054,4.12718622157182,332.325020195409));
#58213=CARTESIAN_POINT('Ctrl Pts',(93.7989728242773,4.05255271617787,332.209869279279));
#58214=CARTESIAN_POINT('Ctrl Pts',(93.7912239392492,3.97311642407947,332.097875083972));
#58215=CARTESIAN_POINT('Ctrl Pts',(93.7834750542211,3.8891868361384,331.989450412947));
#58216=CARTESIAN_POINT('Ctrl Pts',(93.7757179444464,3.80516816446548,331.880910658855));
#58217=CARTESIAN_POINT('Ctrl Pts',(93.7679608346716,3.71664690960338,331.775948306966));
#58218=CARTESIAN_POINT('Ctrl Pts',(93.7602037248969,3.62397294742711,331.674943137506));
#58219=CARTESIAN_POINT('Ctrl Pts',(93.7524424699707,3.53124946324859,331.573883994114));
#58220=CARTESIAN_POINT('Ctrl Pts',(93.7446812150445,3.43436912599131,331.476786523225));
#58221=CARTESIAN_POINT('Ctrl Pts',(93.7369199601184,3.33371765624306,331.383992581458));
#58222=CARTESIAN_POINT('Ctrl Pts',(93.7291462897137,3.23290517694546,331.291050199625));
#58223=CARTESIAN_POINT('Ctrl Pts',(93.721372619309,3.12830980864425,331.202425356489));
#58224=CARTESIAN_POINT('Ctrl Pts',(93.7135989489044,3.02034992193897,331.118419212287));
#58225=CARTESIAN_POINT('Ctrl Pts',(93.7061871447273,2.9174155939345,331.038323574309));
#58226=CARTESIAN_POINT('Ctrl Pts',(93.6987753405503,2.81142316898638,330.962426478851));
#58227=CARTESIAN_POINT('Ctrl Pts',(93.6913635363733,2.70275712280939,330.890950596841));
#58228=CARTESIAN_POINT('Ctrl Pts',(93.6835884575949,2.58876503000877,330.815971468937));
#58229=CARTESIAN_POINT('Ctrl Pts',(93.6758133788164,2.4714703688187,330.745620958636));
#58230=CARTESIAN_POINT('Ctrl Pts',(93.668038300038,2.3512857041024,330.68020387053));
#58231=CARTESIAN_POINT('Ctrl Pts',(93.660272788989,2.23124893426737,330.614867282316));
#58232=CARTESIAN_POINT('Ctrl Pts',(93.6525072779399,2.1083295770204,330.554452222048));
#58233=CARTESIAN_POINT('Ctrl Pts',(93.6447417668909,1.98296980009994,330.499220752537));
#58234=CARTESIAN_POINT('Ctrl Pts',(93.6369839553687,1.85773431776327,330.444044045189));
#58235=CARTESIAN_POINT('Ctrl Pts',(93.6292261438465,1.73006358645143,330.394040857193));
#58236=CARTESIAN_POINT('Ctrl Pts',(93.6214683323243,1.60042473307406,330.349427590472));
#58237=CARTESIAN_POINT('Ctrl Pts',(93.6137163588013,1.47088343704494,330.304847896649));
#58238=CARTESIAN_POINT('Ctrl Pts',(93.6059643852783,1.33937733506883,330.265650177339));
#58239=CARTESIAN_POINT('Ctrl Pts',(93.5982124117553,1.20639358231703,330.232002769816));
#58240=CARTESIAN_POINT('Ctrl Pts',(93.5904637211977,1.07346614826357,330.19836961199));
#58241=CARTESIAN_POINT('Ctrl Pts',(93.58271503064,0.939062686223085,330.17028218653));
#58242=CARTESIAN_POINT('Ctrl Pts',(93.5749663400824,0.803685355365287,330.147858935267));
#58243=CARTESIAN_POINT('Ctrl Pts',(93.5672192617046,0.668336190891868,330.125440349348));
#58244=CARTESIAN_POINT('Ctrl Pts',(93.5594721833268,0.532013946007936,330.108683657381));
#58245=CARTESIAN_POINT('Ctrl Pts',(93.5517251049489,0.395230422856683,330.097656073331));
#58246=CARTESIAN_POINT('Ctrl Pts',(93.5439779616431,0.258445753327946,330.086628396859));
#58247=CARTESIAN_POINT('Ctrl Pts',(93.5362308183373,0.121200187431118,330.081329955484));
#58248=CARTESIAN_POINT('Ctrl Pts',(93.5284836750315,-0.0159903034833192,
330.081775994051));
#58249=CARTESIAN_POINT('Ctrl Pts',(93.5207347900034,-0.153211637732751,
330.082222132896));
#58250=CARTESIAN_POINT('Ctrl Pts',(93.5129859049753,-0.290377481565105,
330.088415320315));
#58251=CARTESIAN_POINT('Ctrl Pts',(93.5052370199472,-0.426973216483055,
330.100318690475));
#58252=CARTESIAN_POINT('Ctrl Pts',(93.4974799101725,-0.563713935525438,
330.112234694996));
#58253=CARTESIAN_POINT('Ctrl Pts',(93.4897228003977,-0.699882946856863,
330.129872955382));
#58254=CARTESIAN_POINT('Ctrl Pts',(93.481965690623,-0.834971547270154,330.153144774418));
#58255=CARTESIAN_POINT('Ctrl Pts',(93.4742044356968,-0.970132334712393,
330.176429029171));
#58256=CARTESIAN_POINT('Ctrl Pts',(93.4664431807707,-1.1042111789492,330.205352758672));
#58257=CARTESIAN_POINT('Ctrl Pts',(93.4586819258445,-1.23671186991421,330.239776600483));
#58258=CARTESIAN_POINT('Ctrl Pts',(93.4509082554399,-1.36942451880271,330.274255509221));
#58259=CARTESIAN_POINT('Ctrl Pts',(93.4431345850352,-1.50055359559283,330.314251997957));
#58260=CARTESIAN_POINT('Ctrl Pts',(93.4353609146305,-1.62961944387752,330.359577225011));
#58261=CARTESIAN_POINT('Ctrl Pts',(93.4279491104535,-1.75267724587232,330.402792551841));
#58262=CARTESIAN_POINT('Ctrl Pts',(93.4205373062764,-1.87385931562098,330.450851569902));
#58263=CARTESIAN_POINT('Ctrl Pts',(93.4131255020994,-1.99277034251709,330.50355146538));
#58264=CARTESIAN_POINT('Ctrl Pts',(93.4053504233209,-2.11750955305984,330.558834339721));
#58265=CARTESIAN_POINT('Ctrl Pts',(93.3975753445425,-2.24014366957103,330.619399224852));
#58266=CARTESIAN_POINT('Ctrl Pts',(93.3898002657641,-2.36019311284394,330.685064133433));
#58267=CARTESIAN_POINT('Ctrl Pts',(93.3820347547151,-2.4800948276341,330.750648237164));
#58268=CARTESIAN_POINT('Ctrl Pts',(93.3742692436661,-2.59741785802978,330.821319691316));
#58269=CARTESIAN_POINT('Ctrl Pts',(93.3665037326171,-2.71170254748708,330.896848484829));
#58270=CARTESIAN_POINT('Ctrl Pts',(93.3587459210949,-2.82587392334213,330.972302391323));
#58271=CARTESIAN_POINT('Ctrl Pts',(93.3509881095727,-2.93701262935733,331.052603838811));
#58272=CARTESIAN_POINT('Ctrl Pts',(93.3432302980505,-3.04468389936381,331.137477117808));
#58273=CARTESIAN_POINT('Ctrl Pts',(93.3354783245275,-3.15227414332494,331.222286526971));
#58274=CARTESIAN_POINT('Ctrl Pts',(93.3277263510045,-3.25640183933689,331.311660678599));
#58275=CARTESIAN_POINT('Ctrl Pts',(93.3199743774815,-3.35666180137882,331.405281010473));
#58276=CARTESIAN_POINT('Ctrl Pts',(93.3122256869239,-3.45687930326736,331.498861694081));
#58277=CARTESIAN_POINT('Ctrl Pts',(93.3044769963663,-3.5532320439348,331.596684715111));
#58278=CARTESIAN_POINT('Ctrl Pts',(93.2967283058087,-3.64534867597783,331.698391892873));
#58279=CARTESIAN_POINT('Ctrl Pts',(93.2889812274308,-3.73744614238625,331.800077909608));
#58280=CARTESIAN_POINT('Ctrl Pts',(93.281234149053,-3.82530899102509,331.905646186116));
#58281=CARTESIAN_POINT('Ctrl Pts',(93.2734870706751,-3.90860373473029,332.01470271039));
#58282=CARTESIAN_POINT('Ctrl Pts',(93.2657399273693,-3.99189917652562,332.123760148663));
#58283=CARTESIAN_POINT('Ctrl Pts',(93.2579927840635,-4.07062619977048,332.236305582379));
#58284=CARTESIAN_POINT('Ctrl Pts',(93.2502456407577,-4.14449276304682,332.351913370082));
#58285=CARTESIAN_POINT('Ctrl Pts',(93.2424967557296,-4.21837593309477,332.467547148869));
#58286=CARTESIAN_POINT('Ctrl Pts',(93.2347478707016,-4.28739625834084,332.58624432233));
#58287=CARTESIAN_POINT('Ctrl Pts',(93.2269989856735,-4.3513062504514,332.707552186574));
#58288=CARTESIAN_POINT('Ctrl Pts',(93.2192418758988,-4.4152840772879,332.828988808238));
#58289=CARTESIAN_POINT('Ctrl Pts',(93.211484766124,-4.47414055324128,332.953041309683));
#58290=CARTESIAN_POINT('Ctrl Pts',(93.2037276563493,-4.52767497719698,333.079233912377));
#58291=CARTESIAN_POINT('Ctrl Pts',(93.1959664014232,-4.58123800823714,333.205493948362));
#58292=CARTESIAN_POINT('Ctrl Pts',(93.188205146497,-4.62947318309786,333.333895998604));
#58293=CARTESIAN_POINT('Ctrl Pts',(93.1804438915708,-4.67222916688808,333.463947372457));
#58294=CARTESIAN_POINT('Ctrl Pts',(93.1726702211662,-4.71505354631822,333.594206786126));
#58295=CARTESIAN_POINT('Ctrl Pts',(93.1648965507615,-4.75238111328922,333.726120419367));
#58296=CARTESIAN_POINT('Ctrl Pts',(93.1571228803569,-4.78411109919153,333.859182725809));
#58297=CARTESIAN_POINT('Ctrl Pts',(93.1497110761798,-4.81436404661656,333.986050949874));
#58298=CARTESIAN_POINT('Ctrl Pts',(93.1422992720026,-4.83952876440203,334.113963029932));
#58299=CARTESIAN_POINT('Ctrl Pts',(93.1348874678254,-4.85956187775862,334.242476786669));
#58300=CARTESIAN_POINT('Ctrl Pts',(93.121960343435,-4.89450216248528,334.466621040822));
#58301=CARTESIAN_POINT('Ctrl Pts',(93.1090332190446,-4.91394075435093,334.693242051901));
#58302=CARTESIAN_POINT('Ctrl Pts',(93.0961060946542,-4.91760996652478,334.920657201737));
#58303=CARTESIAN_POINT('Ctrl Pts',(93.0946765219389,-4.91801573392143,334.945806375166));
#58304=CARTESIAN_POINT('Ctrl Pts',(93.0932469492237,-4.91822868337733,334.970965218337));
#58305=CARTESIAN_POINT('Ctrl Pts',(93.0918173765085,-4.91824847853178,334.996131418882));
#58306=CARTESIAN_POINT('',(91.3418173765403,-4.91824977563263,334.998514405971));
#58307=CARTESIAN_POINT('Ctrl Pts',(93.0918173764786,-4.91824847853219,334.996131419409));
#58308=CARTESIAN_POINT('Ctrl Pts',(93.0841670405432,-4.91835441197591,335.130807946413));
#58309=CARTESIAN_POINT('Ctrl Pts',(93.0765167046078,-4.91292441288391,335.265689551054));
#58310=CARTESIAN_POINT('Ctrl Pts',(93.0688663686724,-4.9019345736358,335.400275527973));
#58311=CARTESIAN_POINT('Ctrl Pts',(93.0612235414835,-4.89095552083125,335.53472940978));
#58312=CARTESIAN_POINT('Ctrl Pts',(93.0535807142946,-4.87442751375331,335.668887841591));
#58313=CARTESIAN_POINT('Ctrl Pts',(93.0459378871057,-4.85237868326861,335.802249447903));
#58314=CARTESIAN_POINT('Ctrl Pts',(93.0380508682076,-4.82962538289751,335.939872016523));
#58315=CARTESIAN_POINT('Ctrl Pts',(93.0301638493095,-4.80099256063041,336.076645554702));
#58316=CARTESIAN_POINT('Ctrl Pts',(93.0222768304114,-4.76656921628651,336.212023501773));
#58317=CARTESIAN_POINT('Ctrl Pts',(93.0146424450639,-4.73324850550022,336.343065081467));
#58318=CARTESIAN_POINT('Ctrl Pts',(93.0070080597165,-4.6945026516089,336.472798683477));
#58319=CARTESIAN_POINT('Ctrl Pts',(92.999373674369,-4.65046431971374,336.600738789925));
#58320=CARTESIAN_POINT('Ctrl Pts',(92.9917404031036,-4.60643241431026,336.728660226137));
#58321=CARTESIAN_POINT('Ctrl Pts',(92.9841071318382,-4.5571096977126,336.854788305704));
#58322=CARTESIAN_POINT('Ctrl Pts',(92.9764738605728,-4.50267839643901,336.978653663667));
#58323=CARTESIAN_POINT('Ctrl Pts',(92.9688399372556,-4.44824244551771,337.102529602495));
#58324=CARTESIAN_POINT('Ctrl Pts',(92.9612060139385,-4.38869720493128,337.224142066119));
#58325=CARTESIAN_POINT('Ctrl Pts',(92.9535720906214,-4.32427240432899,337.34304315702));
#58326=CARTESIAN_POINT('Ctrl Pts',(92.9459357487757,-4.25982719309214,337.46198191737));
#58327=CARTESIAN_POINT('Ctrl Pts',(92.9382994069301,-4.19049954043573,337.578207242644));
#58328=CARTESIAN_POINT('Ctrl Pts',(92.9306630650844,-4.11656403727938,337.691297751918));
#58329=CARTESIAN_POINT('Ctrl Pts',(92.9230185230526,-4.04254913944699,337.80450970196));
#58330=CARTESIAN_POINT('Ctrl Pts',(92.9153739810208,-3.96391673735568,337.914579780392));
#58331=CARTESIAN_POINT('Ctrl Pts',(92.907729438989,-3.88098360102912,338.021117235567));
#58332=CARTESIAN_POINT('Ctrl Pts',(92.9000799730801,-3.79799704717011,338.127723311903));
#58333=CARTESIAN_POINT('Ctrl Pts',(92.8924305071712,-3.71070450560542,338.230791929636));
#58334=CARTESIAN_POINT('Ctrl Pts',(92.8847810412623,-3.61946064865998,338.329968119262));
#58335=CARTESIAN_POINT('Ctrl Pts',(92.8771210068183,-3.52809072880846,338.42928133114));
#58336=CARTESIAN_POINT('Ctrl Pts',(92.8694609723744,-3.43275888576777,338.524691102134));
#58337=CARTESIAN_POINT('Ctrl Pts',(92.8618009379304,-3.33385409106862,338.615881629971));
#58338=CARTESIAN_POINT('Ctrl Pts',(92.8600837698041,-3.31168236818159,338.636324027322));
#58339=CARTESIAN_POINT('Ctrl Pts',(92.8583666016778,-3.28933121214617,338.656554563683));
#58340=CARTESIAN_POINT('Ctrl Pts',(92.8566494335515,-3.26680520479631,338.676569979807));
#58341=CARTESIAN_POINT('Ctrl Pts',(92.848874354773,-3.16481083451602,338.767196770952));
#58342=CARTESIAN_POINT('Ctrl Pts',(92.8410992759946,-3.05888122157502,338.853719305274));
#58343=CARTESIAN_POINT('Ctrl Pts',(92.8333241972162,-2.94938068862535,338.935776494679));
#58344=CARTESIAN_POINT('Ctrl Pts',(92.8255586861672,-2.84001490305284,339.017732707487));
#58345=CARTESIAN_POINT('Ctrl Pts',(92.8177931751182,-2.72708725056083,339.095234276476));
#58346=CARTESIAN_POINT('Ctrl Pts',(92.8100276640692,-2.61099750827896,339.167958142096));
#58347=CARTESIAN_POINT('Ctrl Pts',(92.802269852547,-2.49502286931439,339.240609901791));
#58348=CARTESIAN_POINT('Ctrl Pts',(92.7945120410248,-2.37589270893908,339.308493179057));
#58349=CARTESIAN_POINT('Ctrl Pts',(92.7867542295026,-2.25403808430272,339.371326500848));
#58350=CARTESIAN_POINT('Ctrl Pts',(92.7790022559797,-2.13227515913579,339.434112538571));
#58351=CARTESIAN_POINT('Ctrl Pts',(92.7712502824566,-2.00779219663088,339.491856006617));
#58352=CARTESIAN_POINT('Ctrl Pts',(92.7634983089337,-1.88104700101329,339.544320107836));
#58353=CARTESIAN_POINT('Ctrl Pts',(92.7557496183761,-1.75435548206121,339.596761990477));
#58354=CARTESIAN_POINT('Ctrl Pts',(92.7480009278185,-1.62540399590929,339.643928803986));
#58355=CARTESIAN_POINT('Ctrl Pts',(92.7402522372609,-1.49467238594812,339.685630962974));
#58356=CARTESIAN_POINT('Ctrl Pts',(92.732505158883,-1.36396797579029,339.72732444548));
#58357=CARTESIAN_POINT('Ctrl Pts',(92.7247580805052,-1.23148455066784,339.76355541626));
#58358=CARTESIAN_POINT('Ctrl Pts',(92.7170110021274,-1.09771888014727,339.794183592925));
#58359=CARTESIAN_POINT('Ctrl Pts',(92.7092638588216,-0.963952088541721,
339.824812026283));
#58360=CARTESIAN_POINT('Ctrl Pts',(92.7015167155159,-0.828903411117643,
339.849837484626));
#58361=CARTESIAN_POINT('Ctrl Pts',(92.6937695722101,-0.693081233854145,
339.86917051106));
#58362=CARTESIAN_POINT('Ctrl Pts',(92.686020687182,-0.557228520881242,339.888507883969));
#58363=CARTESIAN_POINT('Ctrl Pts',(92.6782718021538,-0.420602348927069,
339.902150223279));
#58364=CARTESIAN_POINT('Ctrl Pts',(92.6705229171257,-0.283717276389902,
339.910059833605));
#58365=CARTESIAN_POINT('Ctrl Pts',(92.662765807351,-0.14668691262255,339.917977839272));
#58366=CARTESIAN_POINT('Ctrl Pts',(92.6550086975763,-0.0093974901736511,
339.920150938457));
#58367=CARTESIAN_POINT('Ctrl Pts',(92.6472515878016,0.127634815189879,339.916593578531));
#58368=CARTESIAN_POINT('Ctrl Pts',(92.6394903328754,0.26474034623586,339.913034317665));
#58369=CARTESIAN_POINT('Ctrl Pts',(92.6317290779493,0.401588096646474,339.903738522507));
#58370=CARTESIAN_POINT('Ctrl Pts',(92.6239678230231,0.537666950536118,339.888772577325));
#58371=CARTESIAN_POINT('Ctrl Pts',(92.6161941526184,0.67396348624399,339.873782691507));
#58372=CARTESIAN_POINT('Ctrl Pts',(92.6084204822138,0.809488280953241,339.853104589322));
#58373=CARTESIAN_POINT('Ctrl Pts',(92.6006468118091,0.943739467722467,339.826856003608));
#58374=CARTESIAN_POINT('Ctrl Pts',(92.593235007632,1.07174122944952,339.801829295873));
#58375=CARTESIAN_POINT('Ctrl Pts',(92.5858232034549,1.1985850077016,339.771739112013));
#58376=CARTESIAN_POINT('Ctrl Pts',(92.5784113992777,1.32385038664073,339.73672916856));
#58377=CARTESIAN_POINT('Ctrl Pts',(92.5706363204993,1.4552553949473,339.70000328349));
#58378=CARTESIAN_POINT('Ctrl Pts',(92.5628612417208,1.5853386317387,339.657747120043));
#58379=CARTESIAN_POINT('Ctrl Pts',(92.5550861629424,1.71359929444044,339.610071639421));
#58380=CARTESIAN_POINT('Ctrl Pts',(92.5473206518934,1.84170212423134,339.562454826513));
#58381=CARTESIAN_POINT('Ctrl Pts',(92.5395551408444,1.96798647956887,339.509432100346));
#58382=CARTESIAN_POINT('Ctrl Pts',(92.5317896297953,2.0919643504414,339.451164815976));
#58383=CARTESIAN_POINT('Ctrl Pts',(92.5240318182731,2.21581929689341,339.392955303789));
#58384=CARTESIAN_POINT('Ctrl Pts',(92.516274006751,2.33737195843876,339.329511746869));
#58385=CARTESIAN_POINT('Ctrl Pts',(92.5085161952288,2.45615236862982,339.261044309154));
#58386=CARTESIAN_POINT('Ctrl Pts',(92.5007642217058,2.57484339279587,339.192628395357));
#58387=CARTESIAN_POINT('Ctrl Pts',(92.4930122481827,2.69076598082098,339.119196320338));
#58388=CARTESIAN_POINT('Ctrl Pts',(92.4852602746597,2.80347326079535,339.041004916912));
#58389=CARTESIAN_POINT('Ctrl Pts',(92.4775115841021,2.91613280916965,338.962846627592));
#58390=CARTESIAN_POINT('Ctrl Pts',(92.4697628935445,3.02557943730098,338.879933241048));
#58391=CARTESIAN_POINT('Ctrl Pts',(92.4620142029868,3.13139404799926,338.792565672293));
#58392=CARTESIAN_POINT('Ctrl Pts',(92.454267124609,3.23718664308401,338.70521628109));
#58393=CARTESIAN_POINT('Ctrl Pts',(92.4465200462312,3.33934842259777,338.613414799716));
#58394=CARTESIAN_POINT('Ctrl Pts',(92.4387729678533,3.43749258956973,338.517503057448));
#58395=CARTESIAN_POINT('Ctrl Pts',(92.4310258245475,3.53563757908407,338.421590511346));
#58396=CARTESIAN_POINT('Ctrl Pts',(92.4232786812417,3.6297646093454,338.321567908833));
#58397=CARTESIAN_POINT('Ctrl Pts',(92.4155315379359,3.71952333731798,338.217814352266));
#58398=CARTESIAN_POINT('Ctrl Pts',(92.4077826529079,3.80930224495782,338.114037469696));
#58399=CARTESIAN_POINT('Ctrl Pts',(92.4000337678799,3.89471064038191,338.006528259507));
#58400=CARTESIAN_POINT('Ctrl Pts',(92.3922848828518,3.97543836766182,337.895699025697));
#58401=CARTESIAN_POINT('Ctrl Pts',(92.3845277730771,4.0562517801861,337.784752156592));
#58402=CARTESIAN_POINT('Ctrl Pts',(92.3767706633023,4.13237436980426,337.670478540975));
#58403=CARTESIAN_POINT('Ctrl Pts',(92.3690135535276,4.20353895329355,337.553320060361));
#58404=CARTESIAN_POINT('Ctrl Pts',(92.3612522986014,4.27474156486085,337.436098974002));
#58405=CARTESIAN_POINT('Ctrl Pts',(92.3534910436753,4.34098070246503,337.31599029301));
#58406=CARTESIAN_POINT('Ctrl Pts',(92.3457297887491,4.40203559591913,337.193459749975));
#58407=CARTESIAN_POINT('Ctrl Pts',(92.3379561183444,4.46318815730497,337.070733198004));
#58408=CARTESIAN_POINT('Ctrl Pts',(92.3301824479398,4.51913974285814,336.945577399237));
#58409=CARTESIAN_POINT('Ctrl Pts',(92.3224087775351,4.56971776763404,336.818478096285));
#58410=CARTESIAN_POINT('Ctrl Pts',(92.314996973358,4.61794137318849,336.697295296464));
#58411=CARTESIAN_POINT('Ctrl Pts',(92.3075851691809,4.66128034234134,336.574346132178));
#58412=CARTESIAN_POINT('Ctrl Pts',(92.3001733650038,4.69962801825756,336.450061913336));
#58413=CARTESIAN_POINT('Ctrl Pts',(92.2923982862253,4.73985522800213,336.319686154706));
#58414=CARTESIAN_POINT('Ctrl Pts',(92.2846232074469,4.77471662226578,336.187429150985));
#58415=CARTESIAN_POINT('Ctrl Pts',(92.2768481286685,4.80403449768238,336.053772085215));
#58416=CARTESIAN_POINT('Ctrl Pts',(92.2690826176194,4.83331629558679,335.920279492973));
#58417=CARTESIAN_POINT('Ctrl Pts',(92.2613171065704,4.85706806483019,335.785390644839));
#58418=CARTESIAN_POINT('Ctrl Pts',(92.2535515955214,4.87516140210359,335.649603237322));
#58419=CARTESIAN_POINT('Ctrl Pts',(92.2457937839992,4.89323679978045,335.513950463415));
#58420=CARTESIAN_POINT('Ctrl Pts',(92.238035972477,4.90566487911035,335.377401288069));
#58421=CARTESIAN_POINT('Ctrl Pts',(92.2302781609548,4.91236804562007,335.240464647861));
#58422=CARTESIAN_POINT('Ctrl Pts',(92.2225261874318,4.91906616778437,335.103631056818));
#58423=CARTESIAN_POINT('Ctrl Pts',(92.2147742139088,4.92004793331333,334.966410970124));
#58424=CARTESIAN_POINT('Ctrl Pts',(92.2070222403858,4.91528749036846,334.829319158874));
#58425=CARTESIAN_POINT('Ctrl Pts',(92.1992735498282,4.91052906347398,334.692285406087));
#58426=CARTESIAN_POINT('Ctrl Pts',(92.1915248592706,4.90003327837805,334.555380210522));
#58427=CARTESIAN_POINT('Ctrl Pts',(92.1837761687129,4.88382638339658,334.419118842327));
#58428=CARTESIAN_POINT('Ctrl Pts',(92.1760290903351,4.86762286039498,334.282885824447));
#58429=CARTESIAN_POINT('Ctrl Pts',(92.1682820119573,4.84571063714553,334.147296755389));
#58430=CARTESIAN_POINT('Ctrl Pts',(92.1605349335794,4.81816784714409,334.012861884412));
#58431=CARTESIAN_POINT('Ctrl Pts',(92.1527877902736,4.79062482630755,333.878425886741));
#58432=CARTESIAN_POINT('Ctrl Pts',(92.1450406469678,4.75745122304795,333.745144489367));
#58433=CARTESIAN_POINT('Ctrl Pts',(92.137293503662,4.71877624190575,333.613517457259));
#58434=CARTESIAN_POINT('Ctrl Pts',(92.1295446186339,4.6800925658068,333.4818608326));
#58435=CARTESIAN_POINT('Ctrl Pts',(92.1217957336059,4.63590516084678,333.351859688269));
#58436=CARTESIAN_POINT('Ctrl Pts',(92.1140468485778,4.58639289908473,333.223997962353));
#58437=CARTESIAN_POINT('Ctrl Pts',(92.106289738803,4.5368280844964,333.096000522681));
#58438=CARTESIAN_POINT('Ctrl Pts',(92.0985326290283,4.48192726435879,332.970147402637));
#58439=CARTESIAN_POINT('Ctrl Pts',(92.0907755192536,4.42191743809321,332.846902409739));
#58440=CARTESIAN_POINT('Ctrl Pts',(92.0830142643274,4.36187554449522,332.723591558657));
#58441=CARTESIAN_POINT('Ctrl Pts',(92.0752530094013,4.29671939040158,332.602891955577));
#58442=CARTESIAN_POINT('Ctrl Pts',(92.0674917544751,4.22672114886593,332.485241285485));
#58443=CARTESIAN_POINT('Ctrl Pts',(92.0597180840704,4.1566109329562,332.367402412663));
#58444=CARTESIAN_POINT('Ctrl Pts',(92.0519444136658,4.08164336513511,332.252622546546));
#58445=CARTESIAN_POINT('Ctrl Pts',(92.0441707432611,4.00213352111117,332.141309680693));
#58446=CARTESIAN_POINT('Ctrl Pts',(92.036758939084,3.9263248794549,332.035178455526));
#58447=CARTESIAN_POINT('Ctrl Pts',(92.0293471349068,3.84638750719902,331.932198944152));
#58448=CARTESIAN_POINT('Ctrl Pts',(92.0219353307297,3.76262638391469,331.832694243119));
#58449=CARTESIAN_POINT('Ctrl Pts',(92.0141602519513,3.67475987846731,331.728312520281));
#58450=CARTESIAN_POINT('Ctrl Pts',(92.0063851731728,3.5824076432408,331.627424976491));
#58451=CARTESIAN_POINT('Ctrl Pts',(91.9986100943944,3.48587814983359,331.530441442054));
#58452=CARTESIAN_POINT('Ctrl Pts',(91.9908445833453,3.38946744211318,331.433577252032));
#58453=CARTESIAN_POINT('Ctrl Pts',(91.9830790722963,3.2888899772032,331.340607786907));
#58454=CARTESIAN_POINT('Ctrl Pts',(91.9753135612472,3.18449479231876,331.251910355902));
#58455=CARTESIAN_POINT('Ctrl Pts',(91.967555749725,3.08020311556399,331.163300868658));
#58456=CARTESIAN_POINT('Ctrl Pts',(91.9597979382028,2.97210154771474,331.078955237638));
#58457=CARTESIAN_POINT('Ctrl Pts',(91.9520401266806,2.86057607357491,330.999214128475));
#58458=CARTESIAN_POINT('Ctrl Pts',(91.9442881531576,2.74913452589151,330.919533027026));
#58459=CARTESIAN_POINT('Ctrl Pts',(91.9365361796346,2.6342745171893,330.844449776851));
#58460=CARTESIAN_POINT('Ctrl Pts',(91.9287842061116,2.5164149395517,330.774264689489));
#58461=CARTESIAN_POINT('Ctrl Pts',(91.921035515554,2.39860527551512,330.704109325553));
#58462=CARTESIAN_POINT('Ctrl Pts',(91.9132868249963,2.27779890425685,330.638848198219));
#58463=CARTESIAN_POINT('Ctrl Pts',(91.9055381344387,2.15444333190666,330.578738076962));
#58464=CARTESIAN_POINT('Ctrl Pts',(91.8977910560608,2.03111342471351,330.518640462118));
#58465=CARTESIAN_POINT('Ctrl Pts',(91.890043977683,1.90523572255281,330.463691892759));
#58466=CARTESIAN_POINT('Ctrl Pts',(91.8822968993051,1.77728158743122,330.414102789914));
#58467=CARTESIAN_POINT('Ctrl Pts',(91.8745497559993,1.64932637993065,330.364513271464));
#58468=CARTESIAN_POINT('Ctrl Pts',(91.8668026126935,1.51929506921937,330.320283450369));
#58469=CARTESIAN_POINT('Ctrl Pts',(91.8590554693877,1.38767783831432,330.281575127275));
#58470=CARTESIAN_POINT('Ctrl Pts',(91.8513065843596,1.25603101706171,330.242858101728));
#58471=CARTESIAN_POINT('Ctrl Pts',(91.8435576993315,1.12279794104366,330.209665154594));
#58472=CARTESIAN_POINT('Ctrl Pts',(91.8358088143034,0.988482362058231,330.182107755211));
#58473=CARTESIAN_POINT('Ctrl Pts',(91.8280517045287,0.85402421912962,330.154521106119));
#58474=CARTESIAN_POINT('Ctrl Pts',(91.820294594754,0.718481661541847,330.132582032324));
#58475=CARTESIAN_POINT('Ctrl Pts',(91.8125374849792,0.582367557341854,330.116350638031));
#58476=CARTESIAN_POINT('Ctrl Pts',(91.8047762300531,0.446180718116847,330.1001105702));
#58477=CARTESIAN_POINT('Ctrl Pts',(91.7970149751269,0.309422113234143,330.089584289255));
#58478=CARTESIAN_POINT('Ctrl Pts',(91.7892537202008,0.172607089793971,330.084779775529));
#58479=CARTESIAN_POINT('Ctrl Pts',(91.7814800497961,0.035573206903927,330.079967576146));
#58480=CARTESIAN_POINT('Ctrl Pts',(91.7737063793914,-0.101516883821502,
330.080895431666));
#58481=CARTESIAN_POINT('Ctrl Pts',(91.7659327089868,-0.238149586347875,
330.087519176931));
#58482=CARTESIAN_POINT('Ctrl Pts',(91.7585209048098,-0.368422003698419,
330.09383458526));
#58483=CARTESIAN_POINT('Ctrl Pts',(91.7511091006327,-0.498278370715269,
330.105327504411));
#58484=CARTESIAN_POINT('Ctrl Pts',(91.7436972964557,-0.627281946672058,
330.121916316638));
#58485=CARTESIAN_POINT('Ctrl Pts',(91.7359222176773,-0.762608372169753,
330.139318195969));
#58486=CARTESIAN_POINT('Ctrl Pts',(91.7281471388988,-0.897423953735751,
330.162383121948));
#58487=CARTESIAN_POINT('Ctrl Pts',(91.7203720601204,-1.03121712463991,330.191073476923));
#58488=CARTESIAN_POINT('Ctrl Pts',(91.7126065490714,-1.16484565452921,330.21972852659));
#58489=CARTESIAN_POINT('Ctrl Pts',(91.7048410380224,-1.297453898565,330.253995150393));
#58490=CARTESIAN_POINT('Ctrl Pts',(91.6970755269734,-1.42853568530859,330.293784019161));
#58491=CARTESIAN_POINT('Ctrl Pts',(91.6893177154513,-1.55948750407908,330.333533437151));
#58492=CARTESIAN_POINT('Ctrl Pts',(91.6815599039291,-1.68891550586809,330.378794091105));
#58493=CARTESIAN_POINT('Ctrl Pts',(91.6738020924069,-1.81632433915199,330.429425751888));
#58494=CARTESIAN_POINT('Ctrl Pts',(91.6660501188839,-1.94363729324847,330.480019310741));
#58495=CARTESIAN_POINT('Ctrl Pts',(91.6582981453609,-2.06893374152666,330.535975687544));
#58496=CARTESIAN_POINT('Ctrl Pts',(91.6505461718379,-2.19173445906332,330.597105142812));
#58497=CARTESIAN_POINT('Ctrl Pts',(91.6427974812803,-2.31448317042335,330.658208709719));
#58498=CARTESIAN_POINT('Ctrl Pts',(91.6350487907227,-2.43473790403931,330.724480823918));
#58499=CARTESIAN_POINT('Ctrl Pts',(91.627300100165,-2.55204056573768,330.795684120653));
#58500=CARTESIAN_POINT('Ctrl Pts',(91.6195530217872,-2.66931882163763,330.866872602947));
#58501=CARTESIAN_POINT('Ctrl Pts',(91.6118059434094,-2.78364589338849,330.942990024348));
#58502=CARTESIAN_POINT('Ctrl Pts',(91.6040588650315,-2.89458975242904,331.023753877382));
#58503=CARTESIAN_POINT('Ctrl Pts',(91.5963117217258,-3.00553454128576,331.104518407295));
#58504=CARTESIAN_POINT('Ctrl Pts',(91.58856457842,-3.11309574486761,331.189929216467));
#58505=CARTESIAN_POINT('Ctrl Pts',(91.5808174351142,-3.21687203540074,331.279661659156));
#58506=CARTESIAN_POINT('Ctrl Pts',(91.5730685500861,-3.32067165704671,331.369414275602));
#58507=CARTESIAN_POINT('Ctrl Pts',(91.5653196650581,-3.42068437677736,331.463490203323));
#58508=CARTESIAN_POINT('Ctrl Pts',(91.55757078003,-3.51654384864533,331.561526149139));
#58509=CARTESIAN_POINT('Ctrl Pts',(91.5498136702553,-3.61250506674748,331.659666151321));
#58510=CARTESIAN_POINT('Ctrl Pts',(91.5420565604806,-3.70430395729192,331.761774287976));
#58511=CARTESIAN_POINT('Ctrl Pts',(91.5342994507059,-3.79161243504285,331.867451803255));
#58512=CARTESIAN_POINT('Ctrl Pts',(91.5265381957797,-3.87896756765288,331.97318578922));
#58513=CARTESIAN_POINT('Ctrl Pts',(91.5187769408536,-3.96182727017782,332.082492643066));
#58514=CARTESIAN_POINT('Ctrl Pts',(91.5110156859274,-4.03990594789826,332.194943317037));
#58515=CARTESIAN_POINT('Ctrl Pts',(91.5032420155228,-4.11810952605717,332.307573875439));
#58516=CARTESIAN_POINT('Ctrl Pts',(91.4954683451181,-4.1915165868746,332.423357973281));
#58517=CARTESIAN_POINT('Ctrl Pts',(91.4876946747134,-4.25988633349031,332.541839816399));
#58518=CARTESIAN_POINT('Ctrl Pts',(91.4802828705363,-4.32507345195294,332.654806301216));
#58519=CARTESIAN_POINT('Ctrl Pts',(91.4728710663591,-4.38568154239888,332.770224768623));
#58520=CARTESIAN_POINT('Ctrl Pts',(91.465459262182,-4.44154289346483,332.88768378598));
#58521=CARTESIAN_POINT('Ctrl Pts',(91.4570490574045,-4.50492899897717,333.020965017556));
#58522=CARTESIAN_POINT('Ctrl Pts',(91.448638852627,-4.56237957711634,333.157243344602));
#58523=CARTESIAN_POINT('Ctrl Pts',(91.4402286478496,-4.61362440268593,333.295989162757));
#58524=CARTESIAN_POINT('Ctrl Pts',(91.4318462779367,-4.66469962563346,333.434275780315));
#58525=CARTESIAN_POINT('Ctrl Pts',(91.4234639080239,-4.70960995933787,333.575013330719));
#58526=CARTESIAN_POINT('Ctrl Pts',(91.4150815381111,-4.74813305682816,333.717652333743));
#58527=CARTESIAN_POINT('Ctrl Pts',(91.4067160565243,-4.78657854015439,333.860003955748));
#58528=CARTESIAN_POINT('Ctrl Pts',(91.3983505749376,-4.81866236243912,334.004249117229));
#58529=CARTESIAN_POINT('Ctrl Pts',(91.3899850933509,-4.84421074358203,334.149820410581));
#58530=CARTESIAN_POINT('Ctrl Pts',(91.3816465856593,-4.86967674580334,334.294922319745));
#58531=CARTESIAN_POINT('Ctrl Pts',(91.3733080779676,-4.88864928004082,334.441341549971));
#58532=CARTESIAN_POINT('Ctrl Pts',(91.3649695702759,-4.90100499951194,334.588499019128));
#58533=CARTESIAN_POINT('Ctrl Pts',(91.3572521723641,-4.91244037945907,334.72469518122));
#58534=CARTESIAN_POINT('Ctrl Pts',(91.3495347744523,-4.91820839646373,334.861523354464));
#58535=CARTESIAN_POINT('Ctrl Pts',(91.3418173765404,-4.91824977563263,334.998514405971));
#58536=CARTESIAN_POINT('',(89.5918173764638,-4.91824796037091,335.004479152525));
#58537=CARTESIAN_POINT('Ctrl Pts',(91.3418173765086,-4.9182497756328,334.998514406535));
#58538=CARTESIAN_POINT('Ctrl Pts',(91.333865556607,-4.91829241171009,335.139666668237));
#58539=CARTESIAN_POINT('Ctrl Pts',(91.3259137367055,-4.9122541569799,335.280763706402));
#58540=CARTESIAN_POINT('Ctrl Pts',(91.317961916804,-4.90017551578669,335.421263548132));
#58541=CARTESIAN_POINT('Ctrl Pts',(91.310004976711,-4.88808909713424,335.561853857967));
#58542=CARTESIAN_POINT('Ctrl Pts',(91.302048036618,-4.86995457012187,335.701845845342));
#58543=CARTESIAN_POINT('Ctrl Pts',(91.294091096525,-4.84586413341891,335.840704384992));
#58544=CARTESIAN_POINT('Ctrl Pts',(91.2861277333872,-4.82175425030143,335.979675014794));
#58545=CARTESIAN_POINT('Ctrl Pts',(91.2781643702494,-4.7916789355462,336.117510017953));
#58546=CARTESIAN_POINT('Ctrl Pts',(91.2702010071115,-4.75578111746013,336.25368617497));
#58547=CARTESIAN_POINT('Ctrl Pts',(91.2622241741035,-4.71982257892921,336.390092671245));
#58548=CARTESIAN_POINT('Ctrl Pts',(91.2542473410954,-4.67802195195456,336.524834365975));
#58549=CARTESIAN_POINT('Ctrl Pts',(91.2462705080873,-4.63057185807171,336.657403792));
#58550=CARTESIAN_POINT('Ctrl Pts',(91.238286142611,-4.58307695739393,336.790098402415));
#58551=CARTESIAN_POINT('Ctrl Pts',(91.2303017771348,-4.52992208698784,336.920616320105));
#58552=CARTESIAN_POINT('Ctrl Pts',(91.2223174116586,-4.47134716387251,337.04847201656));
#58553=CARTESIAN_POINT('Ctrl Pts',(91.214318496306,-4.41266549991637,337.176560703923));
#58554=CARTESIAN_POINT('Ctrl Pts',(91.2063195809536,-4.34854421160031,337.301977155514));
#58555=CARTESIAN_POINT('Ctrl Pts',(91.198320665601,-4.27926864095019,337.42426132277));
#58556=CARTESIAN_POINT('Ctrl Pts',(91.1946208530367,-4.247225968238,337.480822553699));
#58557=CARTESIAN_POINT('Ctrl Pts',(91.1909210404723,-4.21408117395572,337.536714077698));
#58558=CARTESIAN_POINT('Ctrl Pts',(91.187221227908,-4.17986548399099,337.591892667191));
#58559=CARTESIAN_POINT('Ctrl Pts',(91.1794461491296,-4.10796192663283,337.707849319788));
#58560=CARTESIAN_POINT('Ctrl Pts',(91.1716710703512,-4.03111583639892,337.820994846696));
#58561=CARTESIAN_POINT('Ctrl Pts',(91.1638959915727,-3.94957339143528,337.930879234661));
#58562=CARTESIAN_POINT('Ctrl Pts',(91.1561304805237,-3.86813128964135,338.040628402891));
#58563=CARTESIAN_POINT('Ctrl Pts',(91.1483649694746,-3.78200456269868,338.147124106088));
#58564=CARTESIAN_POINT('Ctrl Pts',(91.1405994584256,-3.69148421830019,338.249942665424));
#58565=CARTESIAN_POINT('Ctrl Pts',(91.1328416469034,-3.60105362508691,338.352659279858));
#58566=CARTESIAN_POINT('Ctrl Pts',(91.1250838353813,-3.50623834029327,338.451705714488));
#58567=CARTESIAN_POINT('Ctrl Pts',(91.1173260238591,-3.40737121512308,338.546689225863));
#58568=CARTESIAN_POINT('Ctrl Pts',(91.1095740503361,-3.30857849060003,338.641601259133));
#58569=CARTESIAN_POINT('Ctrl Pts',(91.1018220768131,-3.20574027559687,338.732456185201));
#58570=CARTESIAN_POINT('Ctrl Pts',(91.0940701032901,-3.0992278015355,338.818896450113));
#58571=CARTESIAN_POINT('Ctrl Pts',(91.0863214127324,-2.99276043556985,338.905300107523));
#58572=CARTESIAN_POINT('Ctrl Pts',(91.0785727221748,-2.88262220829389,338.987292576506));
#58573=CARTESIAN_POINT('Ctrl Pts',(91.0708240316172,-2.76921894245547,339.064555266108));
#58574=CARTESIAN_POINT('Ctrl Pts',(91.0630769532394,-2.65583927111367,339.141801880562));
#58575=CARTESIAN_POINT('Ctrl Pts',(91.0553298748615,-2.53919623524676,339.214320453077));
#58576=CARTESIAN_POINT('Ctrl Pts',(91.0475827964837,-2.41972594495273,339.281834818606));
#58577=CARTESIAN_POINT('Ctrl Pts',(91.0398356531779,-2.30025465338267,339.349349749969));
#58578=CARTESIAN_POINT('Ctrl Pts',(91.0320885098721,-2.17795640041949,339.411860198388));
#58579=CARTESIAN_POINT('Ctrl Pts',(91.0243413665663,-2.05329292869422,339.469135398651));
#58580=CARTESIAN_POINT('Ctrl Pts',(91.0165924815383,-1.92860142997425,339.526423475595));
#58581=CARTESIAN_POINT('Ctrl Pts',(91.0088435965102,-1.80154400947818,339.578473799142));
#58582=CARTESIAN_POINT('Ctrl Pts',(91.0010947114821,-1.67260309159753,339.62510345403));
#58583=CARTESIAN_POINT('Ctrl Pts',(90.9933376017074,-1.543525314494,339.671782602115));
#58584=CARTESIAN_POINT('Ctrl Pts',(90.9855804919326,-1.41256041464631,339.713029455138));
#58585=CARTESIAN_POINT('Ctrl Pts',(90.9778233821579,-1.28020724118315,339.74871061259));
#58586=CARTESIAN_POINT('Ctrl Pts',(90.9700621272317,-1.14778334241584,339.784410836911));
#58587=CARTESIAN_POINT('Ctrl Pts',(90.9623008723055,-1.01397007296683,339.814539353627));
#58588=CARTESIAN_POINT('Ctrl Pts',(90.9545396173794,-0.879276248177881,
339.839013984469));
#58589=CARTESIAN_POINT('Ctrl Pts',(90.9467659469747,-0.744366957165977,
339.863527766745));
#58590=CARTESIAN_POINT('Ctrl Pts',(90.9389922765701,-0.608574683379752,
339.88236953606));
#58591=CARTESIAN_POINT('Ctrl Pts',(90.9312186061654,-0.472414025544393,
339.89550896751));
#58592=CARTESIAN_POINT('Ctrl Pts',(90.9238068019883,-0.342591679088524,
339.908036755264));
#58593=CARTESIAN_POINT('Ctrl Pts',(90.9163949978111,-0.212434760655099,
339.915381129299));
#58594=CARTESIAN_POINT('Ctrl Pts',(90.908983193634,-0.0823872145721554,
339.917559903995));
#58595=CARTESIAN_POINT('Ctrl Pts',(90.9012081148555,0.0540343491349865,
339.919845466928));
#58596=CARTESIAN_POINT('Ctrl Pts',(90.8934330360771,0.190766665418773,339.91645348711));
#58597=CARTESIAN_POINT('Ctrl Pts',(90.8856579572987,0.327298087413861,339.907347453001));
#58598=CARTESIAN_POINT('Ctrl Pts',(90.8778924462496,0.463661498802075,339.898252624447));
#58599=CARTESIAN_POINT('Ctrl Pts',(90.8701269352007,0.599824121505498,339.88345775805));
#58600=CARTESIAN_POINT('Ctrl Pts',(90.8623614241516,0.735272193998754,339.862978291462));
#58601=CARTESIAN_POINT('Ctrl Pts',(90.8546036126294,0.870585969333695,339.842519130326));
#58602=CARTESIAN_POINT('Ctrl Pts',(90.8468458011073,1.00518622037897,339.816386643609));
#58603=CARTESIAN_POINT('Ctrl Pts',(90.8390879895851,1.13856255590235,339.784648196973));
#58604=CARTESIAN_POINT('Ctrl Pts',(90.8313360160621,1.27183852150355,339.752933634525));
#58605=CARTESIAN_POINT('Ctrl Pts',(90.823584042539,1.4038920261332,339.715621599322));
#58606=CARTESIAN_POINT('Ctrl Pts',(90.815832069016,1.53422150041965,339.672830774825));
#58607=CARTESIAN_POINT('Ctrl Pts',(90.8080833784584,1.66449578009646,339.630058072268));
#58608=CARTESIAN_POINT('Ctrl Pts',(90.8003346879008,1.79304711100607,339.581811316949));
#58609=CARTESIAN_POINT('Ctrl Pts',(90.7925859973432,1.91938796924289,339.528259366029));
#58610=CARTESIAN_POINT('Ctrl Pts',(90.7848389189654,2.04570254120884,339.474718557039));
#58611=CARTESIAN_POINT('Ctrl Pts',(90.7770918405876,2.16980719563602,339.415874900411));
#58612=CARTESIAN_POINT('Ctrl Pts',(90.7693447622098,2.29123369524647,339.351945681677));
#58613=CARTESIAN_POINT('Ctrl Pts',(90.761597618904,2.41266121252795,339.288015927154));
#58614=CARTESIAN_POINT('Ctrl Pts',(90.7538504755982,2.53141018435577,339.219000707607));
#58615=CARTESIAN_POINT('Ctrl Pts',(90.7461033322924,2.64703667990872,339.145163431967));
#58616=CARTESIAN_POINT('Ctrl Pts',(90.7383544472643,2.76268917075269,339.07130955614));
#58617=CARTESIAN_POINT('Ctrl Pts',(90.7306055622362,2.87521745905286,338.992631677312));
#58618=CARTESIAN_POINT('Ctrl Pts',(90.7228566772081,2.98420665994171,338.909436490501));
#58619=CARTESIAN_POINT('Ctrl Pts',(90.7150995674334,3.09331154309453,338.826152999459));
#58620=CARTESIAN_POINT('Ctrl Pts',(90.7073424576587,3.19886952383646,338.738342860078));
#58621=CARTESIAN_POINT('Ctrl Pts',(90.6995853478839,3.30049846694625,338.646353374563));
#58622=CARTESIAN_POINT('Ctrl Pts',(90.6918240929578,3.40218171731364,338.554314732808));
#58623=CARTESIAN_POINT('Ctrl Pts',(90.6840628380316,3.49993146808569,338.458092568916));
#58624=CARTESIAN_POINT('Ctrl Pts',(90.6763015831054,3.59340326462794,338.358070285188));
#58625=CARTESIAN_POINT('Ctrl Pts',(90.6685279127008,3.68702458558233,338.257887998402));
#58626=CARTESIAN_POINT('Ctrl Pts',(90.6607542422962,3.7763540224756,338.153893740891));
#58627=CARTESIAN_POINT('Ctrl Pts',(90.6529805718915,3.86108759555049,338.046503839155));
#58628=CARTESIAN_POINT('Ctrl Pts',(90.6455687677144,3.9418768004133,337.944112963181));
#58629=CARTESIAN_POINT('Ctrl Pts',(90.6381569635373,4.01848821819065,337.838635695905));
#58630=CARTESIAN_POINT('Ctrl Pts',(90.6307451593602,4.09069658562617,337.730454999967));
#58631=CARTESIAN_POINT('Ctrl Pts',(90.6229700805817,4.16644410024723,337.616972045869));
#58632=CARTESIAN_POINT('Ctrl Pts',(90.6151950018033,4.23758541409293,337.500155329138));
#58633=CARTESIAN_POINT('Ctrl Pts',(90.6074199230248,4.30381294235502,337.380415346052));
#58634=CARTESIAN_POINT('Ctrl Pts',(90.5996544119758,4.36995897342737,337.260822710637));
#58635=CARTESIAN_POINT('Ctrl Pts',(90.5918889009268,4.43120306279379,337.138314305167));
#58636=CARTESIAN_POINT('Ctrl Pts',(90.5841233898777,4.48728016646518,337.013330516867));
#58637=CARTESIAN_POINT('Ctrl Pts',(90.5763655783556,4.54330166952482,336.888470650358));
#58638=CARTESIAN_POINT('Ctrl Pts',(90.5686077668334,4.5941662231338,336.761140639639));
#58639=CARTESIAN_POINT('Ctrl Pts',(90.5608499553112,4.63965427453192,336.631806139012));
#58640=CARTESIAN_POINT('Ctrl Pts',(90.5530979817882,4.68510809472885,336.502568966698));
#58641=CARTESIAN_POINT('Ctrl Pts',(90.5453460082652,4.72519333689264,336.371330674205));
#58642=CARTESIAN_POINT('Ctrl Pts',(90.5375940347422,4.75973837651114,336.238577268348));
#58643=CARTESIAN_POINT('Ctrl Pts',(90.5298453441846,4.79426878628487,336.105880083637));
#58644=CARTESIAN_POINT('Ctrl Pts',(90.5220966536269,4.82326356186689,335.971669439251));
#58645=CARTESIAN_POINT('Ctrl Pts',(90.5143479630693,4.84660087168616,335.836446682743));
#58646=CARTESIAN_POINT('Ctrl Pts',(90.5066008846915,4.8699333259832,335.701252060458));
#58647=CARTESIAN_POINT('Ctrl Pts',(90.4988538063137,4.88761058938459,335.565046129844));
#58648=CARTESIAN_POINT('Ctrl Pts',(90.4911067279359,4.89956199187121,335.428340227286));
#58649=CARTESIAN_POINT('Ctrl Pts',(90.4833595846301,4.91151349452211,335.291633179));
#58650=CARTESIAN_POINT('Ctrl Pts',(90.4756124413242,4.91773900650009,335.154426539802));
#58651=CARTESIAN_POINT('Ctrl Pts',(90.4678652980184,4.91821979755603,335.017236166278));
#58652=CARTESIAN_POINT('Ctrl Pts',(90.4601164129903,4.918700696704,334.880014949445));
#58653=CARTESIAN_POINT('Ctrl Pts',(90.4523675279622,4.91343430354956,334.742810396358));
#58654=CARTESIAN_POINT('Ctrl Pts',(90.4446186429342,4.90245400646844,334.606137362826));
#58655=CARTESIAN_POINT('Ctrl Pts',(90.4368615331594,4.89146205478653,334.469319263124));
#58656=CARTESIAN_POINT('Ctrl Pts',(90.4291044233847,4.87474411552898,334.333034200173));
#58657=CARTESIAN_POINT('Ctrl Pts',(90.42134731361,4.8523854472342,334.197791464786));
#58658=CARTESIAN_POINT('Ctrl Pts',(90.4135860586838,4.83001483118199,334.062476460006));
#58659=CARTESIAN_POINT('Ctrl Pts',(90.4058248037576,4.80199755977768,333.928205275074));
#58660=CARTESIAN_POINT('Ctrl Pts',(90.3980635488315,4.76846964002803,333.795475050225));
#58661=CARTESIAN_POINT('Ctrl Pts',(90.3902898784268,4.73488808653347,333.662532500273));
#58662=CARTESIAN_POINT('Ctrl Pts',(90.3825162080221,4.69577838079714,333.531136211101));
#58663=CARTESIAN_POINT('Ctrl Pts',(90.3747425376175,4.6513261197662,333.40176710393));
#58664=CARTESIAN_POINT('Ctrl Pts',(90.3673307334404,4.6089431221809,333.278420159822));
#58665=CARTESIAN_POINT('Ctrl Pts',(90.3599189292633,4.56170387199145,333.156916182574));
#58666=CARTESIAN_POINT('Ctrl Pts',(90.3525071250863,4.50980850777866,333.037651843921));
#58667=CARTESIAN_POINT('Ctrl Pts',(90.3447320463078,4.45536959717738,332.91254200476));
#58668=CARTESIAN_POINT('Ctrl Pts',(90.3369569675294,4.39563457491288,332.789501527849));
#58669=CARTESIAN_POINT('Ctrl Pts',(90.3291818887509,4.33078218427259,332.669011210905));
#58670=CARTESIAN_POINT('Ctrl Pts',(90.3214163777019,4.26600959862779,332.548669164966));
#58671=CARTESIAN_POINT('Ctrl Pts',(90.3136508666529,4.19613235780692,332.430871375902));
#58672=CARTESIAN_POINT('Ctrl Pts',(90.3058853556039,4.12137736231394,332.316079043655));
#58673=CARTESIAN_POINT('Ctrl Pts',(90.2981275440818,4.04669648661663,332.20140052834));
#58674=CARTESIAN_POINT('Ctrl Pts',(90.2903697325596,3.96714769270209,332.089721865068));
#58675=CARTESIAN_POINT('Ctrl Pts',(90.2826119210374,3.88300374660957,331.981479672701));
#58676=CARTESIAN_POINT('Ctrl Pts',(90.2748599475143,3.79892312150439,331.873318936016));
#58677=CARTESIAN_POINT('Ctrl Pts',(90.2671079739912,3.71025446612536,331.768589830178));
#58678=CARTESIAN_POINT('Ctrl Pts',(90.2593560004682,3.61731359810144,331.667699684079));
#58679=CARTESIAN_POINT('Ctrl Pts',(90.2516073099106,3.52441209059057,331.566852265016));
#58680=CARTESIAN_POINT('Ctrl Pts',(90.243858619353,3.42724223325535,331.46984085897));
#58681=CARTESIAN_POINT('Ctrl Pts',(90.2361099287953,3.32615968989382,331.377039224636));
#58682=CARTESIAN_POINT('Ctrl Pts',(90.2283628504175,3.2250981775999,331.284256898458));
#58683=CARTESIAN_POINT('Ctrl Pts',(90.2206157720397,3.1201258862679,331.195682865985));
#58684=CARTESIAN_POINT('Ctrl Pts',(90.2128686936619,3.01163456597101,331.111653268605));
#58685=CARTESIAN_POINT('Ctrl Pts',(90.2051215503561,2.90314233641259,331.027622966976));
#58686=CARTESIAN_POINT('Ctrl Pts',(90.1973744070502,2.79113132808707,330.948137415753));
#58687=CARTESIAN_POINT('Ctrl Pts',(90.1896272637445,2.67602519979056,330.873491525201));
#58688=CARTESIAN_POINT('Ctrl Pts',(90.1818783787163,2.5608931931924,330.798828852668));
#58689=CARTESIAN_POINT('Ctrl Pts',(90.1741294936882,2.44266500984922,330.729008218554));
#58690=CARTESIAN_POINT('Ctrl Pts',(90.1663806086601,2.3217916713604,330.664280163883));
#58691=CARTESIAN_POINT('Ctrl Pts',(90.1586234988854,2.20079003666118,330.599483406185));
#58692=CARTESIAN_POINT('Ctrl Pts',(90.1508663891107,2.07713798350429,330.53979021037));
#58693=CARTESIAN_POINT('Ctrl Pts',(90.1431092793359,1.95130992368549,330.485404487196));
#58694=CARTESIAN_POINT('Ctrl Pts',(90.1353480244098,1.82541462537499,330.430989702031));
#58695=CARTESIAN_POINT('Ctrl Pts',(90.1275867694836,1.69734136822776,330.381888180631));
#58696=CARTESIAN_POINT('Ctrl Pts',(90.1198255145574,1.56758180926913,330.338254582911));
#58697=CARTESIAN_POINT('Ctrl Pts',(90.1120518441528,1.43761467730453,330.294551185655));
#58698=CARTESIAN_POINT('Ctrl Pts',(90.1042781737481,1.30595622863437,330.256333299989));
#58699=CARTESIAN_POINT('Ctrl Pts',(90.0965045033434,1.17311131733125,330.223705107549));
#58700=CARTESIAN_POINT('Ctrl Pts',(90.0890926991663,1.04645036860984,330.192595765318));
#58701=CARTESIAN_POINT('Ctrl Pts',(90.0816808949892,0.918711213102214,330.166567484621));
#58702=CARTESIAN_POINT('Ctrl Pts',(90.0742690908122,0.790335727004762,330.145666626495));
#58703=CARTESIAN_POINT('Ctrl Pts',(90.0664940120337,0.655668175922929,330.123741355053));
#58704=CARTESIAN_POINT('Ctrl Pts',(90.0587189332553,0.519874765792876,330.107389547548));
#58705=CARTESIAN_POINT('Ctrl Pts',(90.0509438544768,0.383456537921072,330.096721082171));
#58706=CARTESIAN_POINT('Ctrl Pts',(90.0431783434278,0.247206181363659,330.08606574502));
#58707=CARTESIAN_POINT('Ctrl Pts',(90.0354128323788,0.110332922870522,330.081079864693));
#58708=CARTESIAN_POINT('Ctrl Pts',(90.0276473213298,-0.0266526158047855,
330.08182221747));
#58709=CARTESIAN_POINT('Ctrl Pts',(90.0198895098076,-0.163502332919209,
330.082563834202));
#58710=CARTESIAN_POINT('Ctrl Pts',(90.0121316982855,-0.300463720319841,
330.089022379287));
#58711=CARTESIAN_POINT('Ctrl Pts',(90.0043738867633,-0.437022006536157,
330.101204757463));
#58712=CARTESIAN_POINT('Ctrl Pts',(89.9966219132403,-0.573477528311397,
330.113377968013));
#58713=CARTESIAN_POINT('Ctrl Pts',(89.9888699397173,-0.709530164938046,
330.131266403461));
#58714=CARTESIAN_POINT('Ctrl Pts',(89.9811179661944,-0.844666477822673,
330.154824915058));
#58715=CARTESIAN_POINT('Ctrl Pts',(89.9733692756367,-0.97974556039939,330.178373449612));
#58716=CARTESIAN_POINT('Ctrl Pts',(89.9656205850791,-1.1139087068,330.207587217348));
#58717=CARTESIAN_POINT('Ctrl Pts',(89.9578718945215,-1.24664914527527,330.242369395268));
#58718=CARTESIAN_POINT('Ctrl Pts',(89.9501248161437,-1.37936196599346,330.277144336465));
#58719=CARTESIAN_POINT('Ctrl Pts',(89.9423777377659,-1.5106522896919,330.317485284384));
#58720=CARTESIAN_POINT('Ctrl Pts',(89.934630659388,-1.64002544946506,330.363244713422));
#58721=CARTESIAN_POINT('Ctrl Pts',(89.9268835160823,-1.76939969350948,330.409004525969));
#58722=CARTESIAN_POINT('Ctrl Pts',(89.9191363727764,-1.89685637307775,330.460182779873));
#58723=CARTESIAN_POINT('Ctrl Pts',(89.9113892294706,-2.02191822575249,330.516582804281));
#58724=CARTESIAN_POINT('Ctrl Pts',(89.9036403444425,-2.14700819498795,330.572995508612));
#58725=CARTESIAN_POINT('Ctrl Pts',(89.8958914594144,-2.26970190971158,330.634632158847));
#58726=CARTESIAN_POINT('Ctrl Pts',(89.8881425743862,-2.38954461096502,330.701249063425));
#58727=CARTESIAN_POINT('Ctrl Pts',(89.8803854646115,-2.50951451449913,330.767936675872));
#58728=CARTESIAN_POINT('Ctrl Pts',(89.8726283548368,-2.62662701747445,330.839614911923));
#58729=CARTESIAN_POINT('Ctrl Pts',(89.864871245062,-2.7404539155405,330.915995176386));
#58730=CARTESIAN_POINT('Ctrl Pts',(89.8571099901359,-2.8543416390614,330.992416256021));
#58731=CARTESIAN_POINT('Ctrl Pts',(89.8493487352097,-2.9649399442258,331.073544139606));
#58732=CARTESIAN_POINT('Ctrl Pts',(89.8415874802835,-3.0718527103851,331.159049077611));
#58733=CARTESIAN_POINT('Ctrl Pts',(89.8338138098789,-3.17893650212739,331.244690795651));
#58734=CARTESIAN_POINT('Ctrl Pts',(89.8260401394742,-3.28232267866212,331.334723303072));
#58735=CARTESIAN_POINT('Ctrl Pts',(89.8182664690696,-3.38165042592205,331.428778435974));
#58736=CARTESIAN_POINT('Ctrl Pts',(89.8108546648924,-3.47635444265063,331.518455279812));
#58737=CARTESIAN_POINT('Ctrl Pts',(89.8034428607153,-3.56736916589403,331.611788464687));
#58738=CARTESIAN_POINT('Ctrl Pts',(89.7960310565382,-3.65441648510363,331.708431496094));
#58739=CARTESIAN_POINT('Ctrl Pts',(89.7883327731203,-3.74482833598726,331.808809950295));
#58740=CARTESIAN_POINT('Ctrl Pts',(89.7806344897024,-3.83125922718602,331.91309179026));
#58741=CARTESIAN_POINT('Ctrl Pts',(89.7729362062846,-3.91334805919744,332.020924635046));
#58742=CARTESIAN_POINT('Ctrl Pts',(89.7652500608121,-3.99530746108672,332.128587458917));
#58743=CARTESIAN_POINT('Ctrl Pts',(89.7575639153397,-4.07293819487718,332.239789825614));
#58744=CARTESIAN_POINT('Ctrl Pts',(89.7498777698673,-4.14591691548458,332.354143618335));
#58745=CARTESIAN_POINT('Ctrl Pts',(89.742198603955,-4.21882936628581,332.468393569776));
#58746=CARTESIAN_POINT('Ctrl Pts',(89.7345194380427,-4.28709799008229,332.585788923023));
#58747=CARTESIAN_POINT('Ctrl Pts',(89.7268402721304,-4.35044045679348,332.705909571443));
#58748=CARTESIAN_POINT('Ctrl Pts',(89.7191663354651,-4.41373978947113,332.825948421848));
#58749=CARTESIAN_POINT('Ctrl Pts',(89.7114923987997,-4.47211945116495,332.948708524726));
#58750=CARTESIAN_POINT('Ctrl Pts',(89.7038184621344,-4.52534138480801,333.07374238134));
#58751=CARTESIAN_POINT('Ctrl Pts',(89.6961480088085,-4.57853916004745,333.198719482814));
#58752=CARTESIAN_POINT('Ctrl Pts',(89.6884775554825,-4.62658370907463,333.325967917878));
#58753=CARTESIAN_POINT('Ctrl Pts',(89.6808071021566,-4.66928397564227,333.455017729128));
#58754=CARTESIAN_POINT('Ctrl Pts',(89.6731365065765,-4.71198503411787,333.584069933701));
#58755=CARTESIAN_POINT('Ctrl Pts',(89.6654659109963,-4.74934147416188,333.714923206294));
#58756=CARTESIAN_POINT('Ctrl Pts',(89.6577953154162,-4.78121130484941,333.84708997711));
#58757=CARTESIAN_POINT('Ctrl Pts',(89.6501249457811,-4.81308019677933,333.979252854822));
#58758=CARTESIAN_POINT('Ctrl Pts',(89.642454576146,-4.83946271293504,334.112728763981));
#58759=CARTESIAN_POINT('Ctrl Pts',(89.6347842065108,-4.86026765416642,334.247018331987));
#58760=CARTESIAN_POINT('Ctrl Pts',(89.6271087563662,-4.88108637565981,334.381396847393));
#58761=CARTESIAN_POINT('Ctrl Pts',(89.6194333062215,-4.89632008458264,334.516589702478));
#58762=CARTESIAN_POINT('Ctrl Pts',(89.6117578560768,-4.90592927962572,334.652090578151));
#58763=CARTESIAN_POINT('Ctrl Pts',(89.6051110295541,-4.91425070068513,334.769432336263));
#58764=CARTESIAN_POINT('Ctrl Pts',(89.5984642030313,-4.91835494669348,334.88700484173));
#58765=CARTESIAN_POINT('Ctrl Pts',(89.5918173765086,-4.91824796037164,335.004479151733));
#58766=CARTESIAN_POINT('',(87.8418168890551,-4.92245083146177,334.999291596085));
#58767=CARTESIAN_POINT('Ctrl Pts',(89.5918173764638,-4.91824796037091,335.004479152525));
#58768=CARTESIAN_POINT('Ctrl Pts',(89.5820887354747,-4.91809136959837,335.176420662286));
#58769=CARTESIAN_POINT('Ctrl Pts',(89.5723600944857,-4.90891462743897,335.347960022259));
#58770=CARTESIAN_POINT('Ctrl Pts',(89.5626314534967,-4.89086547025376,335.518283719964));
#58771=CARTESIAN_POINT('Ctrl Pts',(89.5527221300621,-4.8724811001787,335.691770706587));
#58772=CARTESIAN_POINT('Ctrl Pts',(89.5428128066276,-4.844891715429,335.863996613599));
#58773=CARTESIAN_POINT('Ctrl Pts',(89.532903483193,-4.80830183373595,336.034125977912));
#58774=CARTESIAN_POINT('Ctrl Pts',(89.5278666628834,-4.78970352473403,336.120601209352));
#58775=CARTESIAN_POINT('Ctrl Pts',(89.5228298425739,-4.76878061185351,336.206535146784));
#58776=CARTESIAN_POINT('Ctrl Pts',(89.5177930222643,-4.74556462793198,336.291820198255));
#58777=CARTESIAN_POINT('Ctrl Pts',(89.5100179434858,-4.70972731533896,336.423470317391));
#58778=CARTESIAN_POINT('Ctrl Pts',(89.5022428647075,-4.66835092106235,336.553836056142));
#58779=CARTESIAN_POINT('Ctrl Pts',(89.494467785929,-4.62154302049518,336.68241587374));
#58780=CARTESIAN_POINT('Ctrl Pts',(89.48670227488,-4.57479272002955,336.810837465687));
#58781=CARTESIAN_POINT('Ctrl Pts',(89.478936763831,-4.52262434457786,336.937477145472));
#58782=CARTESIAN_POINT('Ctrl Pts',(89.4711712527819,-4.4651959486605,337.06184582415));
#58783=CARTESIAN_POINT('Ctrl Pts',(89.4634134412598,-4.40782449316502,337.186091190921));
#58784=CARTESIAN_POINT('Ctrl Pts',(89.4556556297376,-4.34520355880484,337.308069685023));
#58785=CARTESIAN_POINT('Ctrl Pts',(89.4478978182154,-4.277540129763,337.427309930925));
#58786=CARTESIAN_POINT('Ctrl Pts',(89.4401458446924,-4.20992761959716,337.546460444761));
#58787=CARTESIAN_POINT('Ctrl Pts',(89.4323938711694,-4.13728035992132,337.662876473372));
#58788=CARTESIAN_POINT('Ctrl Pts',(89.4246418976464,-4.05985215875158,337.776109419958));
#58789=CARTESIAN_POINT('Ctrl Pts',(89.4168932070887,-3.98245674847101,337.889294412324));
#58790=CARTESIAN_POINT('Ctrl Pts',(89.4091445165311,-3.90028464391505,337.999298681833));
#58791=CARTESIAN_POINT('Ctrl Pts',(89.4013958259735,-3.81363392192876,338.105701107965));
#58792=CARTESIAN_POINT('Ctrl Pts',(89.3936487475957,-3.72700122834885,338.212081396183));
#58793=CARTESIAN_POINT('Ctrl Pts',(89.3859016692178,-3.63589201745043,338.314861028724));
#58794=CARTESIAN_POINT('Ctrl Pts',(89.37815459084,-3.54064549762043,338.413650908145));
#58795=CARTESIAN_POINT('Ctrl Pts',(89.3704074475342,-3.44539817953299,338.51244161552));
#58796=CARTESIAN_POINT('Ctrl Pts',(89.3626603042284,-3.34601375465022,338.607242221689));
#58797=CARTESIAN_POINT('Ctrl Pts',(89.3549131609226,-3.2428689498613,338.697699830506));
#58798=CARTESIAN_POINT('Ctrl Pts',(89.3471642758945,-3.13970095593051,338.788177776114));
#58799=CARTESIAN_POINT('Ctrl Pts',(89.3394153908663,-3.03277119363023,338.874310523771));
#58800=CARTESIAN_POINT('Ctrl Pts',(89.3316665058383,-2.92248986222626,338.955785139221));
#58801=CARTESIAN_POINT('Ctrl Pts',(89.3239093960635,-2.81209147707757,339.03734623267));
#58802=CARTESIAN_POINT('Ctrl Pts',(89.3161522862888,-2.69833473148445,339.114239084799));
#58803=CARTESIAN_POINT('Ctrl Pts',(89.3083951765141,-2.58165969186645,339.186193533258));
#58804=CARTESIAN_POINT('Ctrl Pts',(89.3006339215879,-2.46492230483782,339.258186431874));
#58805=CARTESIAN_POINT('Ctrl Pts',(89.2928726666617,-2.34526385727184,339.325235477551));
#58806=CARTESIAN_POINT('Ctrl Pts',(89.2851114117355,-2.22314857966914,339.387116758785));
#58807=CARTESIAN_POINT('Ctrl Pts',(89.2773377413308,-2.10083795741956,339.449097029903));
#58808=CARTESIAN_POINT('Ctrl Pts',(89.2695640709262,-1.97606300751493,339.505892855166));
#58809=CARTESIAN_POINT('Ctrl Pts',(89.2617904005215,-1.849308295548,339.557328372031));
#58810=CARTESIAN_POINT('Ctrl Pts',(89.2543785963445,-1.72845404591932,339.606369553211));
#58811=CARTESIAN_POINT('Ctrl Pts',(89.2469667921674,-1.60580047293763,339.650538142507));
#58812=CARTESIAN_POINT('Ctrl Pts',(89.2395549879904,-1.48177815612713,339.689724571713));
#58813=CARTESIAN_POINT('Ctrl Pts',(89.2317799092119,-1.35167713612559,339.730831644544));
#58814=CARTESIAN_POINT('Ctrl Pts',(89.2240048304335,-1.21965866405884,339.766585733493));
#58815=CARTESIAN_POINT('Ctrl Pts',(89.2162297516551,-1.08620271147651,339.796805888514));
#58816=CARTESIAN_POINT('Ctrl Pts',(89.2084642406061,-0.952910984940047,
339.82698885571));
#58817=CARTESIAN_POINT('Ctrl Pts',(89.200698729557,-0.818185675092528,339.851651353144));
#58818=CARTESIAN_POINT('Ctrl Pts',(89.192933218508,-0.682523599630967,339.870661618143));
#58819=CARTESIAN_POINT('Ctrl Pts',(89.1851754069858,-0.546996033512196,
339.889653034408));
#58820=CARTESIAN_POINT('Ctrl Pts',(89.1774175954637,-0.410533934754198,
339.903003317028));
#58821=CARTESIAN_POINT('Ctrl Pts',(89.1696597839415,-0.273645704114665,
339.910631435072));
#58822=CARTESIAN_POINT('Ctrl Pts',(89.1619078104184,-0.136860486209756,
339.918253812716));
#58823=CARTESIAN_POINT('Ctrl Pts',(89.1541558368954,0.000349836585899654,
339.920162575225));
#58824=CARTESIAN_POINT('Ctrl Pts',(89.1464038633724,0.137470679571206,339.916328393706));
#58825=CARTESIAN_POINT('Ctrl Pts',(89.1386551728148,0.274533451798099,339.912495835965));
#58826=CARTESIAN_POINT('Ctrl Pts',(89.1309064822572,0.411506429676223,339.902925182454));
#58827=CARTESIAN_POINT('Ctrl Pts',(89.1231577916996,0.547874177490426,339.887639199873));
#58828=CARTESIAN_POINT('Ctrl Pts',(89.1154107133217,0.68421355285573,339.872356397669));
#58829=CARTESIAN_POINT('Ctrl Pts',(89.1076636349439,0.819947560429564,339.851360675157));
#58830=CARTESIAN_POINT('Ctrl Pts',(89.0999165565661,0.954565434748096,339.824726716953));
#58831=CARTESIAN_POINT('Ctrl Pts',(89.0921694132603,1.08918443729398,339.798092535532));
#58832=CARTESIAN_POINT('Ctrl Pts',(89.0844222699545,1.22268690448518,339.76582010003));
#58833=CARTESIAN_POINT('Ctrl Pts',(89.0766751266487,1.35457220988645,339.728035235772));
#58834=CARTESIAN_POINT('Ctrl Pts',(89.0689262416206,1.48648716590429,339.690241876675));
#58835=CARTESIAN_POINT('Ctrl Pts',(89.0611773565925,1.61678386098025,339.646933730364));
#58836=CARTESIAN_POINT('Ctrl Pts',(89.0534284715644,1.74497715966093,339.59828639547));
#58837=CARTESIAN_POINT('Ctrl Pts',(89.0456713617896,1.87330652403341,339.549587425792));
#58838=CARTESIAN_POINT('Ctrl Pts',(89.037914252015,1.99952766622661,339.495538085927));
#58839=CARTESIAN_POINT('Ctrl Pts',(89.0301571422402,2.12317525576623,339.436362236766));
#58840=CARTESIAN_POINT('Ctrl Pts',(89.0223958873141,2.24688891862431,339.377154765923));
#58841=CARTESIAN_POINT('Ctrl Pts',(89.0146346323879,2.36802594354105,339.312815510453));
#58842=CARTESIAN_POINT('Ctrl Pts',(89.0068733774617,2.48614681679418,339.243613680325));
#58843=CARTESIAN_POINT('Ctrl Pts',(88.9990997070571,2.60445664494892,339.174301149822));
#58844=CARTESIAN_POINT('Ctrl Pts',(88.9913260366524,2.71974035107673,339.100110712484));
#58845=CARTESIAN_POINT('Ctrl Pts',(88.9835523662477,2.83158782236641,339.021354680543));
#58846=CARTESIAN_POINT('Ctrl Pts',(88.9761405620707,2.93822876695884,338.946264760837));
#58847=CARTESIAN_POINT('Ctrl Pts',(88.9687287578935,3.04174596219514,338.867024912678));
#58848=CARTESIAN_POINT('Ctrl Pts',(88.9613169537164,3.14181425854564,338.783937925931));
#58849=CARTESIAN_POINT('Ctrl Pts',(88.953541874938,3.2467872001882,338.696778598461));
#58850=CARTESIAN_POINT('Ctrl Pts',(88.9457667961596,3.34829634681888,338.605110037908));
#58851=CARTESIAN_POINT('Ctrl Pts',(88.9379917173812,3.4459297935382,338.509237940138));
#58852=CARTESIAN_POINT('Ctrl Pts',(88.9302262063322,3.54344309608568,338.413483819088));
#58853=CARTESIAN_POINT('Ctrl Pts',(88.9224606952831,3.63708991202431,338.313536724294));
#58854=CARTESIAN_POINT('Ctrl Pts',(88.9146951842341,3.72649058274801,338.209743136014));
#58855=CARTESIAN_POINT('Ctrl Pts',(88.9069373727119,3.8158026124464,338.106052459379));
#58856=CARTESIAN_POINT('Ctrl Pts',(88.8991795611897,3.9008766217492,337.998523173208));
#58857=CARTESIAN_POINT('Ctrl Pts',(88.8914217496675,3.98136934519541,337.887538952056));
#58858=CARTESIAN_POINT('Ctrl Pts',(88.8836697761445,4.0618014953146,337.77663825005));
#58859=CARTESIAN_POINT('Ctrl Pts',(88.8759178026215,4.1376589932216,337.662288103275));
#58860=CARTESIAN_POINT('Ctrl Pts',(88.8681658290985,4.20863870431525,337.544905365439));
#58861=CARTESIAN_POINT('Ctrl Pts',(88.8604171385409,4.27958835545911,337.427572339262));
#58862=CARTESIAN_POINT('Ctrl Pts',(88.8526684479833,4.34566412657855,337.307209610195));
#58863=CARTESIAN_POINT('Ctrl Pts',(88.8449197574257,4.40660623083631,337.184262939496));
#58864=CARTESIAN_POINT('Ctrl Pts',(88.8371726790478,4.46753565558028,337.061341848878));
#58865=CARTESIAN_POINT('Ctrl Pts',(88.82942560067,4.52333336450984,336.935838235966));
#58866=CARTESIAN_POINT('Ctrl Pts',(88.8216785222922,4.57378575701152,336.808222030465));
#58867=CARTESIAN_POINT('Ctrl Pts',(88.8139313789864,4.62423857235285,336.680604755417));
#58868=CARTESIAN_POINT('Ctrl Pts',(88.8061842356805,4.66934583820442,336.550875215964));
#58869=CARTESIAN_POINT('Ctrl Pts',(88.7984370923747,4.70894244607535,336.419522490857));
#58870=CARTESIAN_POINT('Ctrl Pts',(88.7906882073466,4.74854795610436,336.28814023487));
#58871=CARTESIAN_POINT('Ctrl Pts',(88.7829393223186,4.78264023006099,336.155134441232));
#58872=CARTESIAN_POINT('Ctrl Pts',(88.7751904372905,4.81110439794924,336.021008097193));
#58873=CARTESIAN_POINT('Ctrl Pts',(88.7674333275158,4.8395987779994,335.886739390066));
#58874=CARTESIAN_POINT('Ctrl Pts',(88.759676217741,4.86245303762319,335.751348139634));
#58875=CARTESIAN_POINT('Ctrl Pts',(88.7519191079663,4.87960360919957,335.615346796194));
#58876=CARTESIAN_POINT('Ctrl Pts',(88.7441578530401,4.89676334549302,335.479272777985));
#58877=CARTESIAN_POINT('Ctrl Pts',(88.736396598114,4.9082132879741,335.342588406467));
#58878=CARTESIAN_POINT('Ctrl Pts',(88.7286353431878,4.91394197495463,335.205808963068));
#58879=CARTESIAN_POINT('Ctrl Pts',(88.7208616727831,4.91967982596735,335.068810717135));
#58880=CARTESIAN_POINT('Ctrl Pts',(88.7130880023785,4.91967813278979,334.931717486493));
#58881=CARTESIAN_POINT('Ctrl Pts',(88.7053143319738,4.91397758986589,334.795043153821));
#58882=CARTESIAN_POINT('Ctrl Pts',(88.6979025277968,4.90854240858656,334.664731044216));
#58883=CARTESIAN_POINT('Ctrl Pts',(88.6904907236196,4.89792702391962,334.53479999768));
#58884=CARTESIAN_POINT('Ctrl Pts',(88.6830789194426,4.8822101012541,334.405687296356));
#58885=CARTESIAN_POINT('Ctrl Pts',(88.6753038406641,4.86572284539043,334.270246396934));
#58886=CARTESIAN_POINT('Ctrl Pts',(88.6675287618857,4.84356922099467,334.135278071874));
#58887=CARTESIAN_POINT('Ctrl Pts',(88.6597536831073,4.815783388864,334.001294130366));
#58888=CARTESIAN_POINT('Ctrl Pts',(88.6519881720583,4.78803174896869,333.867475064628));
#58889=CARTESIAN_POINT('Ctrl Pts',(88.6442226610092,4.75466177023629,333.734638351282));
#58890=CARTESIAN_POINT('Ctrl Pts',(88.6364571499602,4.71575936025072,333.603290753697));
#58891=CARTESIAN_POINT('Ctrl Pts',(88.628699338438,4.67689552211791,333.472073387638));
#58892=CARTESIAN_POINT('Ctrl Pts',(88.6209415269157,4.63251027931863,333.342342571464));
#58893=CARTESIAN_POINT('Ctrl Pts',(88.6131837153935,4.58274051133555,333.214594592743));
#58894=CARTESIAN_POINT('Ctrl Pts',(88.6054317418705,4.53300819668123,333.086942748426));
#58895=CARTESIAN_POINT('Ctrl Pts',(88.5976797683475,4.47789956352514,332.961271134258));
#58896=CARTESIAN_POINT('Ctrl Pts',(88.5899277948245,4.4176011095153,332.83806024605));
#58897=CARTESIAN_POINT('Ctrl Pts',(88.5821791042669,4.35732819193649,332.714901537726));
#58898=CARTESIAN_POINT('Ctrl Pts',(88.5744304137093,4.29186999641765,332.594201833017));
#58899=CARTESIAN_POINT('Ctrl Pts',(88.5666817231517,4.22146078754553,332.47642081921));
#58900=CARTESIAN_POINT('Ctrl Pts',(88.5589346447738,4.15106622789738,332.358664310727));
#58901=CARTESIAN_POINT('Ctrl Pts',(88.551187566396,4.07572290427074,332.243825620553));
#58902=CARTESIAN_POINT('Ctrl Pts',(88.5434404880181,3.99571039903277,332.132338675931));
#58903=CARTESIAN_POINT('Ctrl Pts',(88.5356933447123,3.91569722321299,332.020850796941));
#58904=CARTESIAN_POINT('Ctrl Pts',(88.5279462014065,3.83101501563496,331.912715037087));
#58905=CARTESIAN_POINT('Ctrl Pts',(88.5201990581007,3.74198570337721,331.808334908199));
#58906=CARTESIAN_POINT('Ctrl Pts',(88.5124501730726,3.65293637543993,331.703931312442));
#58907=CARTESIAN_POINT('Ctrl Pts',(88.5047012880445,3.55953825166814,331.603285325137));
#58908=CARTESIAN_POINT('Ctrl Pts',(88.4969524030164,3.46215214202312,331.506765738175));
#58909=CARTESIAN_POINT('Ctrl Pts',(88.4891952932417,3.36466266575506,331.410143704327));
#58910=CARTESIAN_POINT('Ctrl Pts',(88.4814381834669,3.26317702608077,331.317657095478));
#58911=CARTESIAN_POINT('Ctrl Pts',(88.4736810736922,3.15809175330003,331.229636683257));
#58912=CARTESIAN_POINT('Ctrl Pts',(88.465919818766,3.0529503263095,331.141569235743));
#58913=CARTESIAN_POINT('Ctrl Pts',(88.4581585638398,2.94420574314074,331.05797297846));
#58914=CARTESIAN_POINT('Ctrl Pts',(88.4503973089137,2.83228511236174,330.979136398136));
#58915=CARTESIAN_POINT('Ctrl Pts',(88.442623638509,2.72018544504841,330.900173704976));
#58916=CARTESIAN_POINT('Ctrl Pts',(88.4348499681043,2.60489990636934,330.825986115296));
#58917=CARTESIAN_POINT('Ctrl Pts',(88.4270762976996,2.48688265333304,330.756817499677));
#58918=CARTESIAN_POINT('Ctrl Pts',(88.4196644935225,2.37435913181912,330.690868699755));
#58919=CARTESIAN_POINT('Ctrl Pts',(88.4122526893455,2.25935274907523,330.629482258468));
#58920=CARTESIAN_POINT('Ctrl Pts',(88.4048408851684,2.1422737953427,330.572828662872));
#58921=CARTESIAN_POINT('Ctrl Pts',(88.39706580639,2.01945645332735,330.513398305793));
#58922=CARTESIAN_POINT('Ctrl Pts',(88.3892907276116,1.89397011202614,330.458988656004));
#58923=CARTESIAN_POINT('Ctrl Pts',(88.3815156488331,1.76626364907357,330.409847956281));
#58924=CARTESIAN_POINT('Ctrl Pts',(88.3737501377841,1.63871433705385,330.360767727317));
#58925=CARTESIAN_POINT('Ctrl Pts',(88.3659846267351,1.50895070059308,330.31694368659));
#58926=CARTESIAN_POINT('Ctrl Pts',(88.3582191156861,1.3774453773434,330.278577831317));
#58927=CARTESIAN_POINT('Ctrl Pts',(88.3504613041639,1.24607044200467,330.240250015901));
#58928=CARTESIAN_POINT('Ctrl Pts',(88.3427034926417,1.11295762929524,330.207369724904));
#58929=CARTESIAN_POINT('Ctrl Pts',(88.3349456811195,0.978598351360524,330.180090423129));
#58930=CARTESIAN_POINT('Ctrl Pts',(88.3271937075965,0.844340183043319,330.152831649893));
#58931=CARTESIAN_POINT('Ctrl Pts',(88.3194417340735,0.708837798069523,330.131165553743));
#58932=CARTESIAN_POINT('Ctrl Pts',(88.3116897605505,0.572596180197431,330.115195328683));
#58933=CARTESIAN_POINT('Ctrl Pts',(88.3039410699929,0.436412260731209,330.099231867022));
#58934=CARTESIAN_POINT('Ctrl Pts',(88.2961923794353,0.299490118440352,330.088959524157));
#58935=CARTESIAN_POINT('Ctrl Pts',(88.2884436888777,0.162343088182089,330.084430065168));
#58936=CARTESIAN_POINT('Ctrl Pts',(88.2806966104998,0.0252245925090398,
330.079901548571));
#58937=CARTESIAN_POINT('Ctrl Pts',(88.272949532122,-0.112118307647133,330.081113552093));
#58938=CARTESIAN_POINT('Ctrl Pts',(88.2652024537442,-0.24916941555038,330.088065791885));
#58939=CARTESIAN_POINT('Ctrl Pts',(88.2574553104384,-0.386221672073916,
330.095018089943));
#58940=CARTESIAN_POINT('Ctrl Pts',(88.2497081671326,-0.522981741094443,
330.107710700426));
#58941=CARTESIAN_POINT('Ctrl Pts',(88.2419610238268,-0.658936087692332,
330.126091271388));
#58942=CARTESIAN_POINT('Ctrl Pts',(88.2342121387987,-0.794920999713729,
330.144475974694));
#58943=CARTESIAN_POINT('Ctrl Pts',(88.2264632537706,-0.930099441582536,
330.168551130739));
#58944=CARTESIAN_POINT('Ctrl Pts',(88.2187143687425,-1.06396603335614,330.198212901183));
#58945=CARTESIAN_POINT('Ctrl Pts',(88.2109572589678,-1.19797471251335,330.227906154937));
#58946=CARTESIAN_POINT('Ctrl Pts',(88.203200149193,-1.33066837788202,330.263197783512));
#58947=CARTESIAN_POINT('Ctrl Pts',(88.1954430394183,-1.46155429124487,330.303933335626));
#58948=CARTESIAN_POINT('Ctrl Pts',(88.1876817844921,-1.59251014585482,330.344690655517));
#58949=CARTESIAN_POINT('Ctrl Pts',(88.1799205295659,-1.72165595576657,330.3908975639));
#58950=CARTESIAN_POINT('Ctrl Pts',(88.1721592746398,-1.84851799338471,330.442351012788));
#58951=CARTESIAN_POINT('Ctrl Pts',(88.1643856042351,-1.97558296891889,330.493886770426));
#58952=CARTESIAN_POINT('Ctrl Pts',(88.1566119338305,-2.1003565158653,330.550685677752));
#58953=CARTESIAN_POINT('Ctrl Pts',(88.1488382634258,-2.22238778783423,330.612497796811));
#58954=CARTESIAN_POINT('Ctrl Pts',(88.1414264592487,-2.33873847473389,330.671432546857));
#58955=CARTESIAN_POINT('Ctrl Pts',(88.1340146550717,-2.45259619560212,330.734924141927));
#58956=CARTESIAN_POINT('Ctrl Pts',(88.1266028508946,-2.56359555264389,330.802719820531));
#58957=CARTESIAN_POINT('Ctrl Pts',(88.1188277721161,-2.68003531882461,330.873838367296));
#58958=CARTESIAN_POINT('Ctrl Pts',(88.1110526933377,-2.79369741379469,330.949918325304));
#58959=CARTESIAN_POINT('Ctrl Pts',(88.1032776145592,-2.90413017146207,331.030716562186));
#58960=CARTESIAN_POINT('Ctrl Pts',(88.0955121035102,-3.0144270345905,331.111415371694));
#58961=CARTESIAN_POINT('Ctrl Pts',(88.0877465924612,-3.12150215490779,331.196820678919));
#58962=CARTESIAN_POINT('Ctrl Pts',(88.0799810814122,-3.2249298972908,331.286644345062));
#58963=CARTESIAN_POINT('Ctrl Pts',(88.07222326989,-3.32825509076612,331.376378950779));
#58964=CARTESIAN_POINT('Ctrl Pts',(88.0644654583678,-3.42793980990432,331.470522942695));
#58965=CARTESIAN_POINT('Ctrl Pts',(88.0567076468456,-3.52358907156986,331.568746130463));
#58966=CARTESIAN_POINT('Ctrl Pts',(88.0489556733226,-3.61916635413291,331.666895402168));
#58967=CARTESIAN_POINT('Ctrl Pts',(88.0412036997996,-3.71071395224622,331.769117480682));
#58968=CARTESIAN_POINT('Ctrl Pts',(88.0334517262765,-3.79787181218263,331.875043558587));
#58969=CARTESIAN_POINT('Ctrl Pts',(88.0257030357189,-3.8849927607135,331.980924776735));
#58970=CARTESIAN_POINT('Ctrl Pts',(88.0179543451613,-3.96772742076359,332.090506573142));
#58971=CARTESIAN_POINT('Ctrl Pts',(88.0102056546037,-4.04575446702686,332.203385286631));
#58972=CARTESIAN_POINT('Ctrl Pts',(88.0024585762258,-4.12376527911147,332.316240514761));
#58973=CARTESIAN_POINT('Ctrl Pts',(87.994711497848,-4.19707020350187,332.432390974235));
#58974=CARTESIAN_POINT('Ctrl Pts',(87.9869644194701,-4.26539013521873,332.551402430599));
#58975=CARTESIAN_POINT('Ctrl Pts',(87.9792172761643,-4.33371063952243,332.670414884393));
#58976=CARTESIAN_POINT('Ctrl Pts',(87.9714701328585,-4.39704587322069,332.792288043915));
#58977=CARTESIAN_POINT('Ctrl Pts',(87.9637229895527,-4.45516195696875,332.916561736053));
#58978=CARTESIAN_POINT('Ctrl Pts',(87.9559741045245,-4.5132911064464,333.040863367556));
#58979=CARTESIAN_POINT('Ctrl Pts',(87.9482252194964,-4.56619860553989,333.167566251597));
#58980=CARTESIAN_POINT('Ctrl Pts',(87.9404763344683,-4.61369828403918,333.296189210518));
#58981=CARTESIAN_POINT('Ctrl Pts',(87.9327192246935,-4.66124837918786,333.424948691176));
#58982=CARTESIAN_POINT('Ctrl Pts',(87.9249621149188,-4.7033790520974,333.555631950535));
#58983=CARTESIAN_POINT('Ctrl Pts',(87.9172050051441,-4.73995353522223,333.687741052065));
#58984=CARTESIAN_POINT('Ctrl Pts',(87.9094437502179,-4.77654756258143,333.819920748475));
#58985=CARTESIAN_POINT('Ctrl Pts',(87.9016824952917,-4.80757939566933,333.953527424713));
#58986=CARTESIAN_POINT('Ctrl Pts',(87.8939212403656,-4.83296342068516,334.088052832222));
#58987=CARTESIAN_POINT('Ctrl Pts',(87.8861475699609,-4.85838805186836,334.22279343654));
#58988=CARTESIAN_POINT('Ctrl Pts',(87.8783738995562,-4.87814676470385,334.358455321969));
#58989=CARTESIAN_POINT('Ctrl Pts',(87.8706002291515,-4.89220575849805,334.494524106392));
#58990=CARTESIAN_POINT('Ctrl Pts',(87.8631884249746,-4.90561030274846,334.624258856162));
#58991=CARTESIAN_POINT('Ctrl Pts',(87.8557766207976,-4.91383381183715,334.754363187925));
#58992=CARTESIAN_POINT('Ctrl Pts',(87.8483648166207,-4.91689110057861,334.884393047134));
#58993=CARTESIAN_POINT('Ctrl Pts',(87.8461823365833,-4.91779134989543,334.922681642625));
#58994=CARTESIAN_POINT('Ctrl Pts',(87.8439998565459,-4.91824436888267,334.960980794805));
#58995=CARTESIAN_POINT('Ctrl Pts',(87.8418173765086,-4.91824994782974,334.999283639204));
#58996=CARTESIAN_POINT('',(86.0918183737958,-4.91614223044281,334.995887905754));
#58997=CARTESIAN_POINT('Ctrl Pts',(87.8418164509476,-4.92622645040437,334.999298747474));
#58998=CARTESIAN_POINT('Ctrl Pts',(87.7512532280806,-4.92298212659158,336.591274825728));
#58999=CARTESIAN_POINT('Ctrl Pts',(87.5679439937889,-3.21788844791034,339.819547858999));
#59000=CARTESIAN_POINT('Ctrl Pts',(87.2918887480729,2.28441556428547,340.348447849244));
#59001=CARTESIAN_POINT('Ctrl Pts',(87.0136507137988,5.73385224213235,335.973338241222));
#59002=CARTESIAN_POINT('Ctrl Pts',(86.735412679525,3.92141734889474,330.70501049568));
#59003=CARTESIAN_POINT('Ctrl Pts',(86.4571746452509,-1.48964436539838,329.378131224311));
#59004=CARTESIAN_POINT('Ctrl Pts',(86.2426434753134,-4.60773713649915,332.332910879143));
#59005=CARTESIAN_POINT('Ctrl Pts',(86.1208583168005,-4.9184828895762,334.482243502733));
#59006=CARTESIAN_POINT('Ctrl Pts',(86.0918191697123,-4.91446141997587,334.995875227902));
#59007=CARTESIAN_POINT('',(84.3418173764577,-4.91824930023121,335.002623599657));
#59008=CARTESIAN_POINT('Ctrl Pts',(86.0918173765086,-4.91824829421748,334.995903791165));
#59009=CARTESIAN_POINT('Ctrl Pts',(86.0838540931834,-4.91836569290393,335.136862397669));
#59010=CARTESIAN_POINT('Ctrl Pts',(86.0758908098582,-4.91241836281413,335.277914761862));
#59011=CARTESIAN_POINT('Ctrl Pts',(86.0679275265329,-4.90041250066869,335.418497772742));
#59012=CARTESIAN_POINT('Ctrl Pts',(86.0602115756372,-4.88877952982098,335.554714401539));
#59013=CARTESIAN_POINT('Ctrl Pts',(86.0524956247415,-4.87145882520636,335.690489980585));
#59014=CARTESIAN_POINT('Ctrl Pts',(86.0447796738458,-4.84850889564337,335.825314819549));
#59015=CARTESIAN_POINT('Ctrl Pts',(86.0370640114249,-4.82555982410478,335.960134617844));
#59016=CARTESIAN_POINT('Ctrl Pts',(86.0293483490039,-4.79698201203871,336.094003358224));
#59017=CARTESIAN_POINT('Ctrl Pts',(86.0216326865829,-4.76288540529612,336.226419862248));
#59018=CARTESIAN_POINT('Ctrl Pts',(86.0139156105548,-4.72878255162301,336.358860626654));
#59019=CARTESIAN_POINT('Ctrl Pts',(86.0061985345267,-4.68915898980021,336.489848243718));
#59020=CARTESIAN_POINT('Ctrl Pts',(85.9984814584986,-4.6441748975198,336.618895482651));
#59021=CARTESIAN_POINT('Ctrl Pts',(85.9907612661606,-4.59917263976184,336.747994833443));
#59022=CARTESIAN_POINT('Ctrl Pts',(85.9830410738225,-4.54880567413809,336.875151875321));
#59023=CARTESIAN_POINT('Ctrl Pts',(85.9753208814845,-4.49328261641219,336.999898595316));
#59024=CARTESIAN_POINT('Ctrl Pts',(85.9675916533351,-4.4376945737923,337.124791320462));
#59025=CARTESIAN_POINT('Ctrl Pts',(85.9598624251856,-4.37693855331885,337.247267732583));
#59026=CARTESIAN_POINT('Ctrl Pts',(85.9521331970362,-4.31126967778069,337.366883357487));
#59027=CARTESIAN_POINT('Ctrl Pts',(85.9443985497762,-4.24555476053018,337.486582847208));
#59028=CARTESIAN_POINT('Ctrl Pts',(85.9366639025161,-4.17492033197678,337.603417219478));
#59029=CARTESIAN_POINT('Ctrl Pts',(85.9289292552561,-4.0996646559619,337.716971249601));
#59030=CARTESIAN_POINT('Ctrl Pts',(85.9211835131052,-4.02430103016177,337.830688166216));
#59031=CARTESIAN_POINT('Ctrl Pts',(85.9134377709543,-3.9443031574284,337.94111503249));
#59032=CARTESIAN_POINT('Ctrl Pts',(85.9056920288034,-3.86000952431726,338.047869671538));
#59033=CARTESIAN_POINT('Ctrl Pts',(85.9040275447699,-3.8418956491454,338.070810196633));
#59034=CARTESIAN_POINT('Ctrl Pts',(85.9023630607365,-3.82358353923497,338.093581283071));
#59035=CARTESIAN_POINT('Ctrl Pts',(85.900698576703,-3.80507676839332,338.116179367292));
#59036=CARTESIAN_POINT('Ctrl Pts',(85.8929234979246,-3.71862859686583,338.221738736756));
#59037=CARTESIAN_POINT('Ctrl Pts',(85.8851484191462,-3.62764789475629,338.323864853333));
#59038=CARTESIAN_POINT('Ctrl Pts',(85.8773733403678,-3.53243756824137,338.422143756328));
#59039=CARTESIAN_POINT('Ctrl Pts',(85.8696078293188,-3.43734440409467,338.520301720877));
#59040=CARTESIAN_POINT('Ctrl Pts',(85.8618423182698,-3.33803224101858,338.614621613574));
#59041=CARTESIAN_POINT('Ctrl Pts',(85.8540768072208,-3.23484498649983,338.704721443755));
#59042=CARTESIAN_POINT('Ctrl Pts',(85.8463189956986,-3.13176004244429,338.794731939692));
#59043=CARTESIAN_POINT('Ctrl Pts',(85.8385611841764,-3.02480794560392,338.880530444486));
#59044=CARTESIAN_POINT('Ctrl Pts',(85.8308033726542,-2.91437004277748,338.961771108515));
#59045=CARTESIAN_POINT('Ctrl Pts',(85.8230513991312,-2.80401524797518,339.042950636367));
#59046=CARTESIAN_POINT('Ctrl Pts',(85.8152994256082,-2.69018018208852,339.119578919857));
#59047=CARTESIAN_POINT('Ctrl Pts',(85.8075474520852,-2.57327964142081,339.191350015156));
#59048=CARTESIAN_POINT('Ctrl Pts',(85.7997987615276,-2.4564286082014,339.263090715354));
#59049=CARTESIAN_POINT('Ctrl Pts',(85.79205007097,-2.3365150147009,339.32997811455));
#59050=CARTESIAN_POINT('Ctrl Pts',(85.7843013804124,-2.21398285695901,339.391749420401));
#59051=CARTESIAN_POINT('Ctrl Pts',(85.7765543020345,-2.09147619305594,339.453507874215));
#59052=CARTESIAN_POINT('Ctrl Pts',(85.7688072236567,-1.9663523973973,339.510152176098));
#59053=CARTESIAN_POINT('Ctrl Pts',(85.7610601452789,-1.83907994594124,339.561465555601));
#59054=CARTESIAN_POINT('Ctrl Pts',(85.7533130019731,-1.71180642781954,339.61277936516));
#59055=CARTESIAN_POINT('Ctrl Pts',(85.7455658586673,-1.58238458050164,339.658762017064));
#59056=CARTESIAN_POINT('Ctrl Pts',(85.7378187153615,-1.45130235615365,339.699245102516));
#59057=CARTESIAN_POINT('Ctrl Pts',(85.7300698303334,-1.32019066173875,339.739737289425));
#59058=CARTESIAN_POINT('Ctrl Pts',(85.7223209453053,-1.1874182208884,339.774727334228));
#59059=CARTESIAN_POINT('Ctrl Pts',(85.7145720602772,-1.05348723334344,339.804096971511));
#59060=CARTESIAN_POINT('Ctrl Pts',(85.7068149505025,-0.919414090064437,
339.833497782031));
#59061=CARTESIAN_POINT('Ctrl Pts',(85.6990578407278,-0.784180326067946,
339.857266184412));
#59062=CARTESIAN_POINT('Ctrl Pts',(85.691300730953,-0.648297950511844,339.875335150517));
#59063=CARTESIAN_POINT('Ctrl Pts',(85.6835394760269,-0.512342963759013,
339.893413772099));
#59064=CARTESIAN_POINT('Ctrl Pts',(85.6757782211007,-0.375739063903513,
339.905786853538));
#59065=CARTESIAN_POINT('Ctrl Pts',(85.6680169661746,-0.239001443181835,
339.912439452315));
#59066=CARTESIAN_POINT('Ctrl Pts',(85.6602432957699,-0.102045086829596,
339.919102693081));
#59067=CARTESIAN_POINT('Ctrl Pts',(85.6524696253652,0.0350450267729754,
339.920027162323));
#59068=CARTESIAN_POINT('Ctrl Pts',(85.6446959549606,0.171754751751551,339.915250081913));
#59069=CARTESIAN_POINT('Ctrl Pts',(85.6372841507834,0.30210060614284,339.910695375746));
#59070=CARTESIAN_POINT('Ctrl Pts',(85.6298723466063,0.432100402124639,339.900958010051));
#59071=CARTESIAN_POINT('Ctrl Pts',(85.6224605424292,0.561316336089136,339.886113694271));
#59072=CARTESIAN_POINT('Ctrl Pts',(85.6146854636507,0.696865527890769,339.870541814355));
#59073=CARTESIAN_POINT('Ctrl Pts',(85.6069103848723,0.831980436468299,339.849300502638));
#59074=CARTESIAN_POINT('Ctrl Pts',(85.5991353060939,0.966149033530582,339.822420461501));
#59075=CARTESIAN_POINT('Ctrl Pts',(85.5913697950449,1.10015252759268,339.795573497967));
#59076=CARTESIAN_POINT('Ctrl Pts',(85.5836042839959,1.23321164755928,339.763101687317));
#59077=CARTESIAN_POINT('Ctrl Pts',(85.5758387729468,1.36481906125792,339.725087511626));
#59078=CARTESIAN_POINT('Ctrl Pts',(85.5680809614246,1.49629598582279,339.687111027102));
#59079=CARTESIAN_POINT('Ctrl Pts',(85.5603231499024,1.62632369544553,339.643603221207));
#59080=CARTESIAN_POINT('Ctrl Pts',(85.5525653383802,1.75440498916578,339.594697617525));
#59081=CARTESIAN_POINT('Ctrl Pts',(85.5448133648572,1.8823898976501,339.545828816861));
#59082=CARTESIAN_POINT('Ctrl Pts',(85.5370613913343,2.0084309420348,339.491570442518));
#59083=CARTESIAN_POINT('Ctrl Pts',(85.5293094178113,2.13204637754787,339.432105741799));
#59084=CARTESIAN_POINT('Ctrl Pts',(85.5215607272537,2.25560946185111,339.372666224415));
#59085=CARTESIAN_POINT('Ctrl Pts',(85.513812036696,2.37674862889893,339.308024935099));
#59086=CARTESIAN_POINT('Ctrl Pts',(85.5060633461384,2.49500261926964,339.238413027577));
#59087=CARTESIAN_POINT('Ctrl Pts',(85.4983162677606,2.61323200591006,339.168815603395));
#59088=CARTESIAN_POINT('Ctrl Pts',(85.4905691893828,2.72857707324962,339.094249816224));
#59089=CARTESIAN_POINT('Ctrl Pts',(85.4828221110049,2.84060201517121,339.014992310566));
#59090=CARTESIAN_POINT('Ctrl Pts',(85.4750749676991,2.95262789596941,338.935734140654));
#59091=CARTESIAN_POINT('Ctrl Pts',(85.4673278243933,3.06133327676036,338.85178439958));
#59092=CARTESIAN_POINT('Ctrl Pts',(85.4595806810875,3.16631248007696,338.763462281066));
#59093=CARTESIAN_POINT('Ctrl Pts',(85.4518317960594,3.27131528494751,338.675120305865));
#59094=CARTESIAN_POINT('Ctrl Pts',(85.4440829110313,3.37258994632697,338.582404248749));
#59095=CARTESIAN_POINT('Ctrl Pts',(85.4363340260032,3.4697652432116,338.485672419993));
#59096=CARTESIAN_POINT('Ctrl Pts',(85.4285769162284,3.56704368296036,338.388837919075));
#59097=CARTESIAN_POINT('Ctrl Pts',(85.4208198064537,3.66021378900941,338.287979408203));
#59098=CARTESIAN_POINT('Ctrl Pts',(85.413062696679,3.74894211843394,338.183491174031));
#59099=CARTESIAN_POINT('Ctrl Pts',(85.4053014417528,3.83771786144074,338.078947104687));
#59100=CARTESIAN_POINT('Ctrl Pts',(85.3975401868266,3.9220468581332,337.970769755316));
#59101=CARTESIAN_POINT('Ctrl Pts',(85.3897789319004,4.00163774294694,337.859384275805));
#59102=CARTESIAN_POINT('Ctrl Pts',(85.3820052614958,4.08135594723767,337.747820615828));
#59103=CARTESIAN_POINT('Ctrl Pts',(85.3742315910911,4.15632067984563,337.633038897963));
#59104=CARTESIAN_POINT('Ctrl Pts',(85.3664579206864,4.22628500760272,337.515491621336));
#59105=CARTESIAN_POINT('Ctrl Pts',(85.3590461165093,4.29299247906989,337.403416198717));
#59106=CARTESIAN_POINT('Ctrl Pts',(85.3516343123323,4.35515446951123,337.288827149546));
#59107=CARTESIAN_POINT('Ctrl Pts',(85.3442225081553,4.41259772395807,337.17213360294));
#59108=CARTESIAN_POINT('Ctrl Pts',(85.3364474293769,4.47285644342027,337.049720558002));
#59109=CARTESIAN_POINT('Ctrl Pts',(85.3286723505985,4.52811260115697,336.924604656233));
#59110=CARTESIAN_POINT('Ctrl Pts',(85.32089727182,4.57811492756779,336.797233087966));
#59111=CARTESIAN_POINT('Ctrl Pts',(85.313131760771,4.62805572293273,336.670018258523));
#59112=CARTESIAN_POINT('Ctrl Pts',(85.305366249722,4.67275540934577,336.540553645877));
#59113=CARTESIAN_POINT('Ctrl Pts',(85.297600738673,4.71200880119516,336.409310512257));
#59114=CARTESIAN_POINT('Ctrl Pts',(85.2898429271508,4.75122327319227,336.278197506587));
#59115=CARTESIAN_POINT('Ctrl Pts',(85.2820851156286,4.7850020856823,336.145309861299));
#59116=CARTESIAN_POINT('Ctrl Pts',(85.2743273041064,4.81318845752591,336.01113794056));
#59117=CARTESIAN_POINT('Ctrl Pts',(85.2665753305834,4.84135361823079,335.877066988446));
#59118=CARTESIAN_POINT('Ctrl Pts',(85.2588233570604,4.86393463504489,335.741714065553));
#59119=CARTESIAN_POINT('Ctrl Pts',(85.2510713835374,4.88082490479422,335.605583446967));
#59120=CARTESIAN_POINT('Ctrl Pts',(85.2433226929797,4.89770802150431,335.469510479778));
#59121=CARTESIAN_POINT('Ctrl Pts',(85.2355740024221,4.90890513651081,335.332660859052));
#59122=CARTESIAN_POINT('Ctrl Pts',(85.2278253118645,4.91436101797314,335.195547558221));
#59123=CARTESIAN_POINT('Ctrl Pts',(85.2200782334867,4.91981576429376,335.058462784957));
#59124=CARTESIAN_POINT('Ctrl Pts',(85.2123311551088,4.91953163750699,334.92111483103));
#59125=CARTESIAN_POINT('Ctrl Pts',(85.204584076731,4.91350543417797,334.784019883314));
#59126=CARTESIAN_POINT('Ctrl Pts',(85.1968369334252,4.90747918034357,334.646923786611));
#59127=CARTESIAN_POINT('Ctrl Pts',(85.1890897901194,4.8957107711446,334.510081090846));
#59128=CARTESIAN_POINT('Ctrl Pts',(85.1813426468136,4.87824908803674,334.374005672894));
#59129=CARTESIAN_POINT('Ctrl Pts',(85.1735937617855,4.86078347917178,334.237899662299));
#59130=CARTESIAN_POINT('Ctrl Pts',(85.1658448767574,4.83762209914363,334.102561660393));
#59131=CARTESIAN_POINT('Ctrl Pts',(85.1580959917293,4.8088653697216,333.968497737088));
#59132=CARTESIAN_POINT('Ctrl Pts',(85.1503388819545,4.78007811760985,333.83429151695));
#59133=CARTESIAN_POINT('Ctrl Pts',(85.1425817721798,4.74568373457853,333.701362459583));
#59134=CARTESIAN_POINT('Ctrl Pts',(85.1348246624051,4.70583333958636,333.57020433539));
#59135=CARTESIAN_POINT('Ctrl Pts',(85.1270634074789,4.66596164981726,333.438976124489));
#59136=CARTESIAN_POINT('Ctrl Pts',(85.1193021525527,4.62062826777559,333.30952110113));
#59137=CARTESIAN_POINT('Ctrl Pts',(85.1115408976266,4.570033036447,333.182314353833));
#59138=CARTESIAN_POINT('Ctrl Pts',(85.1037672272219,4.51935686923727,333.054904117196));
#59139=CARTESIAN_POINT('Ctrl Pts',(85.0959935568172,4.46340219221381,332.929749700533));
#59140=CARTESIAN_POINT('Ctrl Pts',(85.0882198864126,4.40241589183839,332.807303628455));
#59141=CARTESIAN_POINT('Ctrl Pts',(85.0808080822355,4.34426851841768,332.690557450489));
#59142=CARTESIAN_POINT('Ctrl Pts',(85.0733962780583,4.28154756220092,332.576273396933));
#59143=CARTESIAN_POINT('Ctrl Pts',(85.0659844738812,4.21450331038607,332.464818564827));
#59144=CARTESIAN_POINT('Ctrl Pts',(85.0582093951028,4.14417302007551,332.347900999393));
#59145=CARTESIAN_POINT('Ctrl Pts',(85.0504343163243,4.06886266659583,332.233727523917));
#59146=CARTESIAN_POINT('Ctrl Pts',(85.0426592375459,3.98881232544097,332.122751436718));
#59147=CARTESIAN_POINT('Ctrl Pts',(85.0348937264969,3.90886049132738,332.011911912659));
#59148=CARTESIAN_POINT('Ctrl Pts',(85.0271282154479,3.82418050173203,331.904262262147));
#59149=CARTESIAN_POINT('Ctrl Pts',(85.0193627043989,3.73505761341126,331.800230057176));
#59150=CARTESIAN_POINT('Ctrl Pts',(85.0116048928767,3.64602309069343,331.696301000439));
#59151=CARTESIAN_POINT('Ctrl Pts',(85.0038470813545,3.55255468840301,331.59598254642));
#59152=CARTESIAN_POINT('Ctrl Pts',(84.9960892698323,3.45497992095919,331.499671899912));
#59153=CARTESIAN_POINT('Ctrl Pts',(84.9883372963093,3.35747858162235,331.403433730219));
#59154=CARTESIAN_POINT('Ctrl Pts',(84.9805853227863,3.25587730503031,331.311197638309));
#59155=CARTESIAN_POINT('Ctrl Pts',(84.9728333492633,3.15054245776644,331.223326161248));
#59156=CARTESIAN_POINT('Ctrl Pts',(84.9650846587056,3.04525221987286,331.13549189781));
#59157=CARTESIAN_POINT('Ctrl Pts',(84.9573359681481,2.93623185566565,331.052018822717));
#59158=CARTESIAN_POINT('Ctrl Pts',(84.9495872775904,2.82388284633023,330.97323098096));
#59159=CARTESIAN_POINT('Ctrl Pts',(84.9418401992126,2.71155721214464,330.894459531671));
#59160=CARTESIAN_POINT('Ctrl Pts',(84.9340931208348,2.59590463019016,330.820371601054));
#59161=CARTESIAN_POINT('Ctrl Pts',(84.9263460424569,2.47735743945906,330.751249221282));
#59162=CARTESIAN_POINT('Ctrl Pts',(84.9185988991511,2.35880925518849,330.682126262198));
#59163=CARTESIAN_POINT('Ctrl Pts',(84.9108517558453,2.23736675142004,330.61796913385));
#59164=CARTESIAN_POINT('Ctrl Pts',(84.9031046125395,2.11348851074179,330.559014819045));
#59165=CARTESIAN_POINT('Ctrl Pts',(84.8953557275114,1.98958241960477,330.500047250058));
#59166=CARTESIAN_POINT('Ctrl Pts',(84.8876068424833,1.86323985475948,330.446284990126));
#59167=CARTESIAN_POINT('Ctrl Pts',(84.8798579574552,1.7349407251728,330.397917455908));
#59168=CARTESIAN_POINT('Ctrl Pts',(84.8721008476805,1.60650541756431,330.34949858389));
#59169=CARTESIAN_POINT('Ctrl Pts',(84.8643437379057,1.47610976310014,330.306486013944));
#59170=CARTESIAN_POINT('Ctrl Pts',(84.856586628131,1.34425076298466,330.269019874411));
#59171=CARTESIAN_POINT('Ctrl Pts',(84.8488253732048,1.21232130163528,330.231533714172));
#59172=CARTESIAN_POINT('Ctrl Pts',(84.8410641182786,1.07892731643922,330.199599981009));
#59173=CARTESIAN_POINT('Ctrl Pts',(84.8333028633524,0.94457646597386,330.17330772035));
#59174=CARTESIAN_POINT('Ctrl Pts',(84.8255291929477,0.810010697933139,330.146973400644));
#59175=CARTESIAN_POINT('Ctrl Pts',(84.8177555225431,0.67448539249313,330.126298646079));
#59176=CARTESIAN_POINT('Ctrl Pts',(84.8099818521384,0.53851469168353,330.111320731594));
#59177=CARTESIAN_POINT('Ctrl Pts',(84.8025700479614,0.408873459710019,330.097040042632));
#59178=CARTESIAN_POINT('Ctrl Pts',(84.7951582437844,0.278827652596291,330.087937773811));
#59179=CARTESIAN_POINT('Ctrl Pts',(84.7877464396073,0.148821414839618,330.084002110559));
#59180=CARTESIAN_POINT('Ctrl Pts',(84.7799713608289,0.012443184101203,330.079873548727));
#59181=CARTESIAN_POINT('Ctrl Pts',(84.7721962820505,-0.124322480785245,
330.081417812792));
#59182=CARTESIAN_POINT('Ctrl Pts',(84.764421203272,-0.26096447296876,330.088678323878));
#59183=CARTESIAN_POINT('Ctrl Pts',(84.756655692223,-0.39743831848221,330.095929900443));
#59184=CARTESIAN_POINT('Ctrl Pts',(84.748890181174,-0.533788407509145,330.108883707434));
#59185=CARTESIAN_POINT('Ctrl Pts',(84.741124670125,-0.669500816840078,330.1275312501));
#59186=CARTESIAN_POINT('Ctrl Pts',(84.7333668586029,-0.805078666920661,
330.146160303673));
#59187=CARTESIAN_POINT('Ctrl Pts',(84.7256090470807,-0.940019710799557,
330.170471805478));
#59188=CARTESIAN_POINT('Ctrl Pts',(84.7178512355586,-1.07381269364743,330.200405291958));
#59189=CARTESIAN_POINT('Ctrl Pts',(84.7100992620356,-1.20750499303416,330.230316252541));
#59190=CARTESIAN_POINT('Ctrl Pts',(84.7023472885126,-1.34005057113636,330.265840691757));
#59191=CARTESIAN_POINT('Ctrl Pts',(84.6945953149896,-1.47094630081934,330.30686671374));
#59192=CARTESIAN_POINT('Ctrl Pts',(84.686846624432,-1.60178659608265,330.347875361178));
#59193=CARTESIAN_POINT('Ctrl Pts',(84.6790979338744,-1.7309780604082,330.394380840669));
#59194=CARTESIAN_POINT('Ctrl Pts',(84.6713492433168,-1.85803093294256,330.44622089746));
#59195=CARTESIAN_POINT('Ctrl Pts',(84.6636021649389,-1.98505737106589,330.498050168494));
#59196=CARTESIAN_POINT('Ctrl Pts',(84.6558550865611,-2.10994574075779,330.555211661578));
#59197=CARTESIAN_POINT('Ctrl Pts',(84.6481080081833,-2.23222491171074,330.617494437421));
#59198=CARTESIAN_POINT('Ctrl Pts',(84.6403608648775,-2.35450510748066,330.679777735253));
#59199=CARTESIAN_POINT('Ctrl Pts',(84.6326137215717,-2.47417571259869,330.74718222405));
#59200=CARTESIAN_POINT('Ctrl Pts',(84.6248665782659,-2.59078927781674,330.819450516924));
#59201=CARTESIAN_POINT('Ctrl Pts',(84.6171176932378,-2.70742906024019,330.891735057244));
#59202=CARTESIAN_POINT('Ctrl Pts',(84.6093688082097,-2.82101010295721,330.968885371695));
#59203=CARTESIAN_POINT('Ctrl Pts',(84.6016199231816,-2.93111341517882,331.050600398813));
#59204=CARTESIAN_POINT('Ctrl Pts',(84.5938628134069,-3.04133359219369,331.132402159104));
#59205=CARTESIAN_POINT('Ctrl Pts',(84.5861057036322,-3.14806835062554,331.218778077154));
#59206=CARTESIAN_POINT('Ctrl Pts',(84.5783485938575,-3.25093089769393,331.309386045531));
#59207=CARTESIAN_POINT('Ctrl Pts',(84.5705873389313,-3.35384841121836,331.40004243191));
#59208=CARTESIAN_POINT('Ctrl Pts',(84.5628260840052,-3.45288930824588,331.494935104525));
#59209=CARTESIAN_POINT('Ctrl Pts',(84.555064829079,-3.54770398539075,331.593685350038));
#59210=CARTESIAN_POINT('Ctrl Pts',(84.5472911586743,-3.64267033511916,331.692593563762));
#59211=CARTESIAN_POINT('Ctrl Pts',(84.5395174882697,-3.73339669652386,331.7953713884));
#59212=CARTESIAN_POINT('Ctrl Pts',(84.531743817865,-3.81957349255914,331.901606642558));
#59213=CARTESIAN_POINT('Ctrl Pts',(84.5243320136879,-3.90173873800721,332.002896620078));
#59214=CARTESIAN_POINT('Ctrl Pts',(84.5169202095106,-3.97976827830493,332.107329153741));
#59215=CARTESIAN_POINT('Ctrl Pts',(84.5095084053335,-4.0534316965053,332.21452435942));
#59216=CARTESIAN_POINT('Ctrl Pts',(84.5016248252933,-4.13178393565423,332.328542750043));
#59217=CARTESIAN_POINT('Ctrl Pts',(84.4937412452531,-4.20543972543899,332.446041085973));
#59218=CARTESIAN_POINT('Ctrl Pts',(84.4858576652129,-4.27407965357783,332.566601927885));
#59219=CARTESIAN_POINT('Ctrl Pts',(84.4779844568314,-4.34262927884607,332.687004159635));
#59220=CARTESIAN_POINT('Ctrl Pts',(84.47011124845,-4.40617599182058,332.810460554398));
#59221=CARTESIAN_POINT('Ctrl Pts',(84.4622380400685,-4.46444249803971,332.936523262986));
#59222=CARTESIAN_POINT('Ctrl Pts',(84.454373654175,-4.52264371250896,333.062444709375));
#59223=CARTESIAN_POINT('Ctrl Pts',(84.4465092682815,-4.57557634175535,333.190966316337));
#59224=CARTESIAN_POINT('Ctrl Pts',(84.4386448823881,-4.62300815605339,333.321614272116));
#59225=CARTESIAN_POINT('Ctrl Pts',(84.4305759235648,-4.67167379398992,333.455660717675));
#59226=CARTESIAN_POINT('Ctrl Pts',(84.4225069647415,-4.71454830376636,333.591945312942));
#59227=CARTESIAN_POINT('Ctrl Pts',(84.4144380059182,-4.75143234417331,333.729931599778));
#59228=CARTESIAN_POINT('Ctrl Pts',(84.4065875903808,-4.78731740075063,333.86418060437));
#59229=CARTESIAN_POINT('Ctrl Pts',(84.3987371748433,-4.81753218104775,334.000039923139));
#59230=CARTESIAN_POINT('Ctrl Pts',(84.3908867593059,-4.84194286277766,334.136998043979));
#59231=CARTESIAN_POINT('Ctrl Pts',(84.3827085288397,-4.86737287728747,334.279675214519));
#59232=CARTESIAN_POINT('Ctrl Pts',(84.3745302983735,-4.88650344351115,334.423544538267));
#59233=CARTESIAN_POINT('Ctrl Pts',(84.3663520679073,-4.89924191044213,334.568014160571));
#59234=CARTESIAN_POINT('Ctrl Pts',(84.358173837441,-4.91198037737311,334.712483782875));
#59235=CARTESIAN_POINT('Ctrl Pts',(84.3499956069748,-4.91832668679319,334.857553244037));
#59236=CARTESIAN_POINT('Ctrl Pts',(84.3418173765086,-4.9182493002317,335.002623598754));
#59237=CARTESIAN_POINT('',(82.5918173765463,-4.91824909607723,335.002981851016));
#59238=CARTESIAN_POINT('Ctrl Pts',(84.3418173764577,-4.91824930023122,335.002623599657));
#59239=CARTESIAN_POINT('Ctrl Pts',(84.3332528523107,-4.91816825833526,335.15454626326));
#59240=CARTESIAN_POINT('Ctrl Pts',(84.3246883281636,-4.91104390444931,335.306222086739));
#59241=CARTESIAN_POINT('Ctrl Pts',(84.3161238040166,-4.89696912524936,335.457030030583));
#59242=CARTESIAN_POINT('Ctrl Pts',(84.3075123360255,-4.88281719941171,335.608664582477));
#59243=CARTESIAN_POINT('Ctrl Pts',(84.2989008680343,-4.86163853326073,335.759421483946));
#59244=CARTESIAN_POINT('Ctrl Pts',(84.2902894000431,-4.83357773483632,335.908685503238));
#59245=CARTESIAN_POINT('Ctrl Pts',(84.2816536082752,-4.80543767645363,336.058371130631));
#59246=CARTESIAN_POINT('Ctrl Pts',(84.2730178165074,-4.77037667053886,336.206555215299));
#59247=CARTESIAN_POINT('Ctrl Pts',(84.2643820247396,-4.72858930711563,336.352636768365));
#59248=CARTESIAN_POINT('Ctrl Pts',(84.2557148909255,-4.68665028400532,336.499248498038));
#59249=CARTESIAN_POINT('Ctrl Pts',(84.2470477571114,-4.63793611011578,336.643742196788));
#59250=CARTESIAN_POINT('Ctrl Pts',(84.2383806232973,-4.5826907614107,336.785533099044));
#59251=CARTESIAN_POINT('Ctrl Pts',(84.236010539218,-4.56758356170332,336.82430674293));
#59252=CARTESIAN_POINT('Ctrl Pts',(84.2336404551387,-4.55198823657263,336.862878416919));
#59253=CARTESIAN_POINT('Ctrl Pts',(84.2312703710595,-4.53591036852141,336.901236490087));
#59254=CARTESIAN_POINT('Ctrl Pts',(84.223495292281,-4.48316680056935,337.027070439727));
#59255=CARTESIAN_POINT('Ctrl Pts',(84.2157202135026,-4.42509964498674,337.150906772384));
#59256=CARTESIAN_POINT('Ctrl Pts',(84.2079451347242,-4.3618811326319,337.272262319207));
#59257=CARTESIAN_POINT('Ctrl Pts',(84.2001796236752,-4.29874041468121,337.393468530305));
#59258=CARTESIAN_POINT('Ctrl Pts',(84.1924141126262,-4.23046113175489,337.512199686352));
#59259=CARTESIAN_POINT('Ctrl Pts',(84.1846486015771,-4.15726393231983,337.627991563824));
#59260=CARTESIAN_POINT('Ctrl Pts',(84.1768907900549,-4.08413930812106,337.743668633314));
#59261=CARTESIAN_POINT('Ctrl Pts',(84.1691329785327,-4.0061066786973,337.85641189559));
#59262=CARTESIAN_POINT('Ctrl Pts',(84.1613751670105,-3.923432885982,337.965781086273));
#59263=CARTESIAN_POINT('Ctrl Pts',(84.1536231934875,-3.8408213079174,338.075067973172));
#59264=CARTESIAN_POINT('Ctrl Pts',(84.1458712199645,-3.75357575320992,338.180985531866));
#59265=CARTESIAN_POINT('Ctrl Pts',(84.1381192464415,-3.66200650719316,338.283122203601));
#59266=CARTESIAN_POINT('Ctrl Pts',(84.1303705558839,-3.57047604080659,338.385215620393));
#59267=CARTESIAN_POINT('Ctrl Pts',(84.1226218653262,-3.47462578539216,338.483531044486));
#59268=CARTESIAN_POINT('Ctrl Pts',(84.1148731747686,-3.37480632238623,338.577689945884));
#59269=CARTESIAN_POINT('Ctrl Pts',(84.1071260963908,-3.27500762765328,338.671829256737));
#59270=CARTESIAN_POINT('Ctrl Pts',(84.0993790180129,-3.17124165211249,338.761813497001));
#59271=CARTESIAN_POINT('Ctrl Pts',(84.0916319396351,-3.06389556843324,338.847301262994));
#59272=CARTESIAN_POINT('Ctrl Pts',(84.0838847963293,-2.95654858509048,338.932789745456));
#59273=CARTESIAN_POINT('Ctrl Pts',(84.0761376530235,-2.84562173952397,339.013781434981));
#59274=CARTESIAN_POINT('Ctrl Pts',(84.0683905097177,-2.73153466729184,339.089975724119));
#59275=CARTESIAN_POINT('Ctrl Pts',(84.0606416246896,-2.61742194586382,339.166187143351));
#59276=CARTESIAN_POINT('Ctrl Pts',(84.0528927396615,-2.50014790896661,339.237598798944));
#59277=CARTESIAN_POINT('Ctrl Pts',(84.0451438546334,-2.3801601519419,339.303954078938));
#59278=CARTESIAN_POINT('Ctrl Pts',(84.0373867448587,-2.2600450386721,339.370379789112));
#59279=CARTESIAN_POINT('Ctrl Pts',(84.0296296350839,-2.13721079405819,339.431738213363));
#59280=CARTESIAN_POINT('Ctrl Pts',(84.0218725253092,-2.01212903153014,339.487819049714));
#59281=CARTESIAN_POINT('Ctrl Pts',(84.014111270383,-1.88698042930755,339.54392985387));
#59282=CARTESIAN_POINT('Ctrl Pts',(84.0063500154569,-1.75958227892961,339.594757305905));
#59283=CARTESIAN_POINT('Ctrl Pts',(83.9985887605307,-1.63042410291557,339.640140117187));
#59284=CARTESIAN_POINT('Ctrl Pts',(83.990815090126,-1.50105931591254,339.685595526178));
#59285=CARTESIAN_POINT('Ctrl Pts',(83.9830414197214,-1.36992925120473,339.725588775866));
#59286=CARTESIAN_POINT('Ctrl Pts',(83.9752677493167,-1.23753730917189,339.760008872986));
#59287=CARTESIAN_POINT('Ctrl Pts',(83.9678559451397,-1.11130824389287,339.792826706304));
#59288=CARTESIAN_POINT('Ctrl Pts',(83.9604441409626,-0.983932419435646,
339.820578509659));
#59289=CARTESIAN_POINT('Ctrl Pts',(83.9530323367856,-0.855851045273139,
339.843211956007));
#59290=CARTESIAN_POINT('Ctrl Pts',(83.9452572580071,-0.721492021427351,
339.866954734982));
#59291=CARTESIAN_POINT('Ctrl Pts',(83.9374821792287,-0.58593193758518,339.885139770372));
#59292=CARTESIAN_POINT('Ctrl Pts',(83.9297071004502,-0.449670304741494,
339.897650424391));
#59293=CARTESIAN_POINT('Ctrl Pts',(83.9219415894012,-0.313576350512047,
339.910145683253));
#59294=CARTESIAN_POINT('Ctrl Pts',(83.9141760783522,-0.176782950518166,
339.916980418895));
#59295=CARTESIAN_POINT('Ctrl Pts',(83.9064105673032,-0.0397998857711188,
339.918088961334));
#59296=CARTESIAN_POINT('Ctrl Pts',(83.898652755781,0.0970473598686024,339.919196404649));
#59297=CARTESIAN_POINT('Ctrl Pts',(83.8908949442588,0.234083507681419,339.914588950238));
#59298=CARTESIAN_POINT('Ctrl Pts',(83.8831371327366,0.370793926475477,339.904252738857));
#59299=CARTESIAN_POINT('Ctrl Pts',(83.8753851592136,0.507401466343871,339.893924305803));
#59300=CARTESIAN_POINT('Ctrl Pts',(83.8676331856906,0.643683376903208,339.877875726105));
#59301=CARTESIAN_POINT('Ctrl Pts',(83.8598812121676,0.779125656416427,339.856145207262));
#59302=CARTESIAN_POINT('Ctrl Pts',(83.8521325216099,0.914510576043951,339.834423891306));
#59303=CARTESIAN_POINT('Ctrl Pts',(83.8443838310523,1.04905618672202,339.807025483967));
#59304=CARTESIAN_POINT('Ctrl Pts',(83.8366351404947,1.18225445477238,339.774039952354));
#59305=CARTESIAN_POINT('Ctrl Pts',(83.8288880621168,1.31542500981058,339.741061283656));
#59306=CARTESIAN_POINT('Ctrl Pts',(83.821140983739,1.44724840063401,339.702497896775));
#59307=CARTESIAN_POINT('Ctrl Pts',(83.8133939053612,1.57722801225449,339.658490620347));
#59308=CARTESIAN_POINT('Ctrl Pts',(83.8056467620553,1.70720871322922,339.614482975095));
#59309=CARTESIAN_POINT('Ctrl Pts',(83.7978996187495,1.83534523394945,339.565031474641));
#59310=CARTESIAN_POINT('Ctrl Pts',(83.7901524754437,1.96115769831933,339.510326323541));
#59311=CARTESIAN_POINT('Ctrl Pts',(83.7824035904156,2.0869984480022,339.45560887356));
#59312=CARTESIAN_POINT('Ctrl Pts',(83.7746547053875,2.21051374323885,339.395635578443));
#59313=CARTESIAN_POINT('Ctrl Pts',(83.7669058203594,2.33124557403613,339.330643963204));
#59314=CARTESIAN_POINT('Ctrl Pts',(83.7591487105847,2.45210555084611,339.265583365194));
#59315=CARTESIAN_POINT('Ctrl Pts',(83.75139160081,2.57017581681137,339.195493992452));
#59316=CARTESIAN_POINT('Ctrl Pts',(83.7436344910352,2.68502430742466,339.120658628307));
#59317=CARTESIAN_POINT('Ctrl Pts',(83.7358732361091,2.79993416939919,339.045783274536));
#59318=CARTESIAN_POINT('Ctrl Pts',(83.7281119811829,2.91161850744542,338.966157102737));
#59319=CARTESIAN_POINT('Ctrl Pts',(83.7203507262567,3.01967678178837,338.882104480308));
#59320=CARTESIAN_POINT('Ctrl Pts',(83.712577055852,3.12790791415415,338.797917401076));
#59321=CARTESIAN_POINT('Ctrl Pts',(83.7048033854474,3.23250109329111,338.709289974345));
#59322=CARTESIAN_POINT('Ctrl Pts',(83.6970297150427,3.33309056376183,338.616585455407));
#59323=CARTESIAN_POINT('Ctrl Pts',(83.6896179108657,3.42899757018056,338.528196354131));
#59324=CARTESIAN_POINT('Ctrl Pts',(83.6822061066887,3.52126502111687,338.436101399095));
#59325=CARTESIAN_POINT('Ctrl Pts',(83.6747943025117,3.60961014988057,338.340643295591));
#59326=CARTESIAN_POINT('Ctrl Pts',(83.6670192237332,3.70228533657253,338.240506506079));
#59327=CARTESIAN_POINT('Ctrl Pts',(83.6592441449548,3.79093686059564,338.136352105636));
#59328=CARTESIAN_POINT('Ctrl Pts',(83.6514690661764,3.87519632468573,338.028537024314));
#59329=CARTESIAN_POINT('Ctrl Pts',(83.6437035551274,3.95935210214103,337.920854616314));
#59330=CARTESIAN_POINT('Ctrl Pts',(83.6359380440784,4.03912633509538,337.809520795533));
#59331=CARTESIAN_POINT('Ctrl Pts',(83.6281725330294,4.1141879285028,337.694928709903));
#59332=CARTESIAN_POINT('Ctrl Pts',(83.6204147215072,4.18917509812181,337.58045024266));
#59333=CARTESIAN_POINT('Ctrl Pts',(83.612656909985,4.25945871412599,337.462720264469));
#59334=CARTESIAN_POINT('Ctrl Pts',(83.6048990984628,4.3247486255139,337.342164039647));
#59335=CARTESIAN_POINT('Ctrl Pts',(83.5971471249398,4.38998940417298,337.221698537207));
#59336=CARTESIAN_POINT('Ctrl Pts',(83.5893951514168,4.45024377278173,337.098411363829));
#59337=CARTESIAN_POINT('Ctrl Pts',(83.5816431778938,4.5052657050071,336.972755430809));
#59338=CARTESIAN_POINT('Ctrl Pts',(83.5738944873362,4.56026433541155,336.847152713151));
#59339=CARTESIAN_POINT('Ctrl Pts',(83.5661457967786,4.61003478032397,336.719183588396));
#59340=CARTESIAN_POINT('Ctrl Pts',(83.558397106221,4.6543777688322,336.589323959267));
#59341=CARTESIAN_POINT('Ctrl Pts',(83.5506500278431,4.69871153141132,336.459491348519));
#59342=CARTESIAN_POINT('Ctrl Pts',(83.5429029494653,4.73761995746883,336.327769385439));
#59343=CARTESIAN_POINT('Ctrl Pts',(83.5351558710875,4.77095272594241,336.194651894621));
#59344=CARTESIAN_POINT('Ctrl Pts',(83.5274087277816,4.80428577377668,336.061533288151));
#59345=CARTESIAN_POINT('Ctrl Pts',(83.5196615844759,4.83204297587769,335.927019509783));
#59346=CARTESIAN_POINT('Ctrl Pts',(83.5119144411701,4.85412459082211,335.791617028162));
#59347=CARTESIAN_POINT('Ctrl Pts',(83.504165556142,4.87621117018238,335.656184105188));
#59348=CARTESIAN_POINT('Ctrl Pts',(83.4964166711139,4.89261956040267,335.519862467085));
#59349=CARTESIAN_POINT('Ctrl Pts',(83.4886677860858,4.90330164584888,335.383165802644));
#59350=CARTESIAN_POINT('Ctrl Pts',(83.4809106763111,4.91399506937095,335.24632404695));
#59351=CARTESIAN_POINT('Ctrl Pts',(83.4731535665364,4.91895001632563,335.109106860064));
#59352=CARTESIAN_POINT('Ctrl Pts',(83.4653964567616,4.91817047034942,334.972030604531));
#59353=CARTESIAN_POINT('Ctrl Pts',(83.4576352018355,4.91739050780877,334.83488109983));
#59354=CARTESIAN_POINT('Ctrl Pts',(83.4498739469093,4.91086996495655,334.697873066777));
#59355=CARTESIAN_POINT('Ctrl Pts',(83.4421126919831,4.89866485420154,334.561518861625));
#59356=CARTESIAN_POINT('Ctrl Pts',(83.4343390215785,4.88644021924696,334.424946534183));
#59357=CARTESIAN_POINT('Ctrl Pts',(83.4265653511738,4.86851289611195,334.289030512404));
#59358=CARTESIAN_POINT('Ctrl Pts',(83.4187916807692,4.84499042266779,334.154274946122));
#59359=CARTESIAN_POINT('Ctrl Pts',(83.411379876592,4.82256292602124,334.025792283868));
#59360=CARTESIAN_POINT('Ctrl Pts',(83.4039680724147,4.79504952557784,333.898364751355));
#59361=CARTESIAN_POINT('Ctrl Pts',(83.3965562682375,4.76258538824808,333.772415590623));
#59362=CARTESIAN_POINT('Ctrl Pts',(83.3887811894591,4.72853008684265,333.640293286342));
#59363=CARTESIAN_POINT('Ctrl Pts',(83.3810061106806,4.68891885594517,333.509380406035));
#59364=CARTESIAN_POINT('Ctrl Pts',(83.3732310319022,4.64385248475392,333.380179898154));
#59365=CARTESIAN_POINT('Ctrl Pts',(83.3654655208532,4.5988415706015,333.251138379723));
#59366=CARTESIAN_POINT('Ctrl Pts',(83.3577000098042,4.54838900039974,333.123805406565));
#59367=CARTESIAN_POINT('Ctrl Pts',(83.3499344987552,4.4926462061047,332.998672158473));
#59368=CARTESIAN_POINT('Ctrl Pts',(83.3421766872329,4.43695868095249,332.87366298036));
#59369=CARTESIAN_POINT('Ctrl Pts',(83.3344188757107,4.37599152812549,332.750849541683));
#59370=CARTESIAN_POINT('Ctrl Pts',(83.3266610641885,4.30994534410407,332.630705971532));
#59371=CARTESIAN_POINT('Ctrl Pts',(83.3189090906655,4.24394886193057,332.510652813227));
#59372=CARTESIAN_POINT('Ctrl Pts',(83.3111571171425,4.17288114386934,332.393265865461));
#59373=CARTESIAN_POINT('Ctrl Pts',(83.3034051436195,4.09698991372582,332.278997113319));
#59374=CARTESIAN_POINT('Ctrl Pts',(83.2956564530618,4.02113082356338,332.16477675406));
#59375=CARTESIAN_POINT('Ctrl Pts',(83.2879077625042,3.94045250002448,332.053672288855));
#59376=CARTESIAN_POINT('Ctrl Pts',(83.2801590719466,3.85524730293788,331.946108827137));
#59377=CARTESIAN_POINT('Ctrl Pts',(83.2724119935687,3.77005983350412,331.838567744895));
#59378=CARTESIAN_POINT('Ctrl Pts',(83.2646649151909,3.68034760648996,331.734566506921));
#59379=CARTESIAN_POINT('Ctrl Pts',(83.2569178368131,3.58644454217906,331.634498758227));
#59380=CARTESIAN_POINT('Ctrl Pts',(83.2491706935072,3.4925406908701,331.534430170869));
#59381=CARTESIAN_POINT('Ctrl Pts',(83.2414235502014,3.39444619967918,331.438295423574));
#59382=CARTESIAN_POINT('Ctrl Pts',(83.2336764068956,3.29253299308747,331.346452470279));
#59383=CARTESIAN_POINT('Ctrl Pts',(83.2259275218675,3.19059687424331,331.254588868738));
#59384=CARTESIAN_POINT('Ctrl Pts',(83.2181786368394,3.08484062192922,331.167019242833));
#59385=CARTESIAN_POINT('Ctrl Pts',(83.2104297518113,2.97567016987738,331.084062040507));
#59386=CARTESIAN_POINT('Ctrl Pts',(83.2026726420365,2.86638384317972,331.001016786549));
#59387=CARTESIAN_POINT('Ctrl Pts',(83.1949155322618,2.75367638943808,330.9225939726));
#59388=CARTESIAN_POINT('Ctrl Pts',(83.1871584224871,2.63798418470832,330.84906968214));
#59389=CARTESIAN_POINT('Ctrl Pts',(83.1793971675609,2.52223015776348,330.77550610265));
#59390=CARTESIAN_POINT('Ctrl Pts',(83.1716359126347,2.40348853994487,330.70684645804));
#59391=CARTESIAN_POINT('Ctrl Pts',(83.1638746577085,2.28222049408427,330.643320911648));
#59392=CARTESIAN_POINT('Ctrl Pts',(83.1561009873039,2.16075845887154,330.579693745085));
#59393=CARTESIAN_POINT('Ctrl Pts',(83.1483273168992,2.03676227329839,330.521217255328));
#59394=CARTESIAN_POINT('Ctrl Pts',(83.1405536464946,1.91071408262761,330.46807383589));
#59395=CARTESIAN_POINT('Ctrl Pts',(83.1331418423176,1.79053346556021,330.417404255412));
#59396=CARTESIAN_POINT('Ctrl Pts',(83.1257300381407,1.66848785522842,330.371582511186));
#59397=CARTESIAN_POINT('Ctrl Pts',(83.1183182339637,1.5450063114647,330.330723979027));
#59398=CARTESIAN_POINT('Ctrl Pts',(83.1105431551853,1.41547256940628,330.287862848494));
#59399=CARTESIAN_POINT('Ctrl Pts',(83.1027680764069,1.28394922552208,330.250328306311));
#59400=CARTESIAN_POINT('Ctrl Pts',(83.0949929976284,1.15091376271326,330.218307770956));
#59401=CARTESIAN_POINT('Ctrl Pts',(83.0872274865794,1.01804200851096,330.186326638909));
#59402=CARTESIAN_POINT('Ctrl Pts',(83.0794619755304,0.883662214148742,330.15984610341));
#59403=CARTESIAN_POINT('Ctrl Pts',(83.0716964644814,0.748269371713734,330.139004627666));
#59404=CARTESIAN_POINT('Ctrl Pts',(83.0639386529592,0.613010771676187,330.118183816306));
#59405=CARTESIAN_POINT('Ctrl Pts',(83.056180841437,0.476741506293891,330.102990997093));
#59406=CARTESIAN_POINT('Ctrl Pts',(83.0484230299148,0.33996883509979,330.093514062625));
#59407=CARTESIAN_POINT('Ctrl Pts',(83.0406710563918,0.203299089678165,330.08404425985));
#59408=CARTESIAN_POINT('Ctrl Pts',(83.0329190828688,0.0661270808542804,
330.080281807033));
#59409=CARTESIAN_POINT('Ctrl Pts',(83.0251671093458,-0.0710330499077727,
330.082262983005));
#59410=CARTESIAN_POINT('Ctrl Pts',(83.0174184187882,-0.208135093273016,
330.084243319948));
#59411=CARTESIAN_POINT('Ctrl Pts',(83.0096697282306,-0.345224878561342,
330.091962442113));
#59412=CARTESIAN_POINT('Ctrl Pts',(83.001921037673,-0.481786709502685,330.10540454899));
#59413=CARTESIAN_POINT('Ctrl Pts',(82.9941739592951,-0.618320127614607,
330.118843859125));
#59414=CARTESIAN_POINT('Ctrl Pts',(82.9864268809173,-0.754325421119501,
330.13800374729));
#59415=CARTESIAN_POINT('Ctrl Pts',(82.9786798025395,-0.889290862103369,
330.162816436698));
#59416=CARTESIAN_POINT('Ctrl Pts',(82.9709326592337,-1.02425743422744,330.18762933406));
#59417=CARTESIAN_POINT('Ctrl Pts',(82.9631855159279,-1.15818375201624,330.218095056485));
#59418=CARTESIAN_POINT('Ctrl Pts',(82.9554383726221,-1.29056753469086,330.254094554155));
#59419=CARTESIAN_POINT('Ctrl Pts',(82.947689487594,-1.42298108005033,330.290102145276));
#59420=CARTESIAN_POINT('Ctrl Pts',(82.939940602566,-1.55385102310939,330.331645884736));
#59421=CARTESIAN_POINT('Ctrl Pts',(82.9321917175379,-1.68268990016405,330.378556744654));
#59422=CARTESIAN_POINT('Ctrl Pts',(82.9244346077631,-1.81166552813415,330.425517396243));
#59423=CARTESIAN_POINT('Ctrl Pts',(82.9166774979884,-1.9386054158323,330.477856414074));
#59424=CARTESIAN_POINT('Ctrl Pts',(82.9089203882137,-2.06304125064884,330.535356244825));
#59425=CARTESIAN_POINT('Ctrl Pts',(82.9011591332875,-2.18754357999674,330.592886801647));
#59426=CARTESIAN_POINT('Ctrl Pts',(82.8933978783614,-2.30953884273251,330.655583487924));
#59427=CARTESIAN_POINT('Ctrl Pts',(82.8856366234352,-2.42858392792535,330.72318305658));
#59428=CARTESIAN_POINT('Ctrl Pts',(82.8778629530306,-2.54781944645781,330.790890762516));
#59429=CARTESIAN_POINT('Ctrl Pts',(82.8700892826259,-2.6640950251489,330.863516816319));
#59430=CARTESIAN_POINT('Ctrl Pts',(82.8623156122213,-2.77699636893558,330.940754475347));
#59431=CARTESIAN_POINT('Ctrl Pts',(82.8549038080441,-2.88464212800749,331.014396702765));
#59432=CARTESIAN_POINT('Ctrl Pts',(82.847492003867,-2.98922049302006,331.092230685172));
#59433=CARTESIAN_POINT('Ctrl Pts',(82.8400801996898,-3.09040225309415,331.173958053475));
#59434=CARTESIAN_POINT('Ctrl Pts',(82.8324063694531,-3.19516104478746,331.258574691349));
#59435=CARTESIAN_POINT('Ctrl Pts',(82.8247325392163,-3.29662844556156,331.347647886257));
#59436=CARTESIAN_POINT('Ctrl Pts',(82.8170587089795,-3.39439409141408,331.440888901049));
#59437=CARTESIAN_POINT('Ctrl Pts',(82.8093943689736,-3.49203883042911,331.534014604619));
#59438=CARTESIAN_POINT('Ctrl Pts',(82.8017300289677,-3.58599063092221,331.631297602963));
#59439=CARTESIAN_POINT('Ctrl Pts',(82.7940656889617,-3.67587032862144,331.732407554535));
#59440=CARTESIAN_POINT('Ctrl Pts',(82.7864088789718,-3.76566172183942,331.833418168191));
#59441=CARTESIAN_POINT('Ctrl Pts',(82.7787520689819,-3.85138870493917,331.938247957744));
#59442=CARTESIAN_POINT('Ctrl Pts',(82.7710952589921,-3.9327076603401,332.046528564417));
#59443=CARTESIAN_POINT('Ctrl Pts',(82.7634440899739,-4.01396670594483,332.154729397942));
#59444=CARTESIAN_POINT('Ctrl Pts',(82.7557929209558,-4.09082394509794,332.266375669851));
#59445=CARTESIAN_POINT('Ctrl Pts',(82.7481417519376,-4.16297523965459,332.381065060655));
#59446=CARTESIAN_POINT('Ctrl Pts',(82.740493585754,-4.23509821717846,332.495709439609));
#59447=CARTESIAN_POINT('Ctrl Pts',(82.7328454195705,-4.30251870852421,332.613394223232));
#59448=CARTESIAN_POINT('Ctrl Pts',(82.7251972533869,-4.36497543862418,332.733687470205));
#59449=CARTESIAN_POINT('Ctrl Pts',(82.7175503313811,-4.4274220084746,332.853961148278));
#59450=CARTESIAN_POINT('Ctrl Pts',(82.7099034093753,-4.48490623804694,332.976842089059));
#59451=CARTESIAN_POINT('Ctrl Pts',(82.7022564873696,-4.53721269882533,333.101873558448));
#59452=CARTESIAN_POINT('Ctrl Pts',(82.6946090521321,-4.58952267021037,333.226913419465));
#59453=CARTESIAN_POINT('Ctrl Pts',(82.6869616168946,-4.63665402759163,333.354103724897));
#59454=CARTESIAN_POINT('Ctrl Pts',(82.6793141816571,-4.67843961371987,333.482968080996));
#59455=CARTESIAN_POINT('Ctrl Pts',(82.6716604408377,-4.7202596535479,333.611938690334));
#59456=CARTESIAN_POINT('Ctrl Pts',(82.6640067000182,-4.75672499409276,333.742585724375));
#59457=CARTESIAN_POINT('Ctrl Pts',(82.6563529591987,-4.78771841246239,333.874417721591));
#59458=CARTESIAN_POINT('Ctrl Pts',(82.6486959875867,-4.81872491375561,334.006305367652));
#59459=CARTESIAN_POINT('Ctrl Pts',(82.6410390159747,-4.84425481630877,334.139378578565));
#59460=CARTESIAN_POINT('Ctrl Pts',(82.6333820443626,-4.86424235210448,334.273137287727));
#59461=CARTESIAN_POINT('Ctrl Pts',(82.6257145787911,-4.88425728102653,334.407079314595));
#59462=CARTESIAN_POINT('Ctrl Pts',(82.6180471132196,-4.89871462721325,334.54170831678));
#59463=CARTESIAN_POINT('Ctrl Pts',(82.6103796476481,-4.90760062330737,334.676520194428));
#59464=CARTESIAN_POINT('Ctrl Pts',(82.6041922239475,-4.91477136601546,334.785309493721));
#59465=CARTESIAN_POINT('Ctrl Pts',(82.5980048002468,-4.91831503790099,334.894217760072));
#59466=CARTESIAN_POINT('Ctrl Pts',(82.5918173765462,-4.91824909607723,335.002981851016));
#59467=CARTESIAN_POINT('',(80.8418173764668,-4.91824819243925,334.995783358204));
#59468=CARTESIAN_POINT('Ctrl Pts',(82.5918173765086,-4.91824909607683,335.002981851677));
#59469=CARTESIAN_POINT('Ctrl Pts',(82.5818256394777,-4.9181426101563,335.178619119737));
#59470=CARTESIAN_POINT('Ctrl Pts',(82.5718339024468,-4.9086284126831,335.353969158787));
#59471=CARTESIAN_POINT('Ctrl Pts',(82.561842165416,-4.8897942842515,335.528294349962));
#59472=CARTESIAN_POINT('Ctrl Pts',(82.5540670866375,-4.87513849098686,335.663945647655));
#59473=CARTESIAN_POINT('Ctrl Pts',(82.5462920078591,-4.85481046140537,335.799200973084));
#59474=CARTESIAN_POINT('Ctrl Pts',(82.5385169290807,-4.82883743807289,335.933548102224));
#59475=CARTESIAN_POINT('Ctrl Pts',(82.5307514180316,-4.80289637619914,336.067729908668));
#59476=CARTESIAN_POINT('Ctrl Pts',(82.5229859069826,-4.77132421564953,336.201005362415));
#59477=CARTESIAN_POINT('Ctrl Pts',(82.5152203959336,-4.73420000922789,336.332866585644));
#59478=CARTESIAN_POINT('Ctrl Pts',(82.5074625844114,-4.69711261156494,336.464597068086));
#59479=CARTESIAN_POINT('Ctrl Pts',(82.4997047728891,-4.65448422827802,336.594915736672));
#59480=CARTESIAN_POINT('Ctrl Pts',(82.4919469613669,-4.6064450209568,336.723324499739));
#59481=CARTESIAN_POINT('Ctrl Pts',(82.4841949878439,-4.55844196466258,336.851636631141));
#59482=CARTESIAN_POINT('Ctrl Pts',(82.4764430143209,-4.50503632549459,336.978041353209));
#59483=CARTESIAN_POINT('Ctrl Pts',(82.4686910407979,-4.44640809204299,337.102055694199));
#59484=CARTESIAN_POINT('Ctrl Pts',(82.4609423502403,-4.3878046876831,337.226017515042));
#59485=CARTESIAN_POINT('Ctrl Pts',(82.4531936596826,-4.3239832548095,337.347590615617));
#59486=CARTESIAN_POINT('Ctrl Pts',(82.445444969125,-4.25517182573731,337.46631218542));
#59487=CARTESIAN_POINT('Ctrl Pts',(82.4376978907472,-4.18637471345766,337.585009054209));
#59488=CARTESIAN_POINT('Ctrl Pts',(82.4299508123693,-4.1125898659386,337.700855234346));
#59489=CARTESIAN_POINT('Ctrl Pts',(82.4222037339915,-4.03409097718606,337.81341306073));
#59490=CARTESIAN_POINT('Ctrl Pts',(82.4144565906857,-3.95559143053722,337.925971830457));
#59491=CARTESIAN_POINT('Ctrl Pts',(82.4067094473799,-3.87237798744675,338.035241870854));
#59492=CARTESIAN_POINT('Ctrl Pts',(82.3989623040741,-3.78476709371294,338.140815357331));
#59493=CARTESIAN_POINT('Ctrl Pts',(82.391213419046,-3.69713650319018,338.24641257897));
#59494=CARTESIAN_POINT('Ctrl Pts',(82.3834645340179,-3.60510674430559,338.348311292231));
#59495=CARTESIAN_POINT('Ctrl Pts',(82.3757156489898,-3.50903361129608,338.446137863942));
#59496=CARTESIAN_POINT('Ctrl Pts',(82.3679585392151,-3.41285850527058,338.544068269787));
#59497=CARTESIAN_POINT('Ctrl Pts',(82.3602014294403,-3.31263172640043,338.637917620737));
#59498=CARTESIAN_POINT('Ctrl Pts',(82.3524443196656,-3.20874529969669,338.727349817789));
#59499=CARTESIAN_POINT('Ctrl Pts',(82.3446830647394,-3.10480335940817,338.816829804548));
#59500=CARTESIAN_POINT('Ctrl Pts',(82.3369218098133,-2.99719818106671,338.901887691862));
#59501=CARTESIAN_POINT('Ctrl Pts',(82.3291605548871,-2.8863529364766,338.982229248624));
#59502=CARTESIAN_POINT('Ctrl Pts',(82.3213868844824,-2.7753303756196,339.062699325693));
#59503=CARTESIAN_POINT('Ctrl Pts',(82.3136132140778,-2.66105771722564,339.138437779826));
#59504=CARTESIAN_POINT('Ctrl Pts',(82.3058395436731,-2.5439857818845,339.209194626537));
#59505=CARTESIAN_POINT('Ctrl Pts',(82.298427739496,-2.43236357329969,339.27665772501));
#59506=CARTESIAN_POINT('Ctrl Pts',(82.291015935319,-2.31819708756365,339.339592427523));
#59507=CARTESIAN_POINT('Ctrl Pts',(82.2836041311419,-2.20189427399635,339.397822719101));
#59508=CARTESIAN_POINT('Ctrl Pts',(82.2758290523635,-2.07989111308739,339.458907050729));
#59509=CARTESIAN_POINT('Ctrl Pts',(82.2680539735851,-1.95515136116017,339.515007194513));
#59510=CARTESIAN_POINT('Ctrl Pts',(82.2602788948066,-1.82812050083908,339.565868865497));
#59511=CARTESIAN_POINT('Ctrl Pts',(82.2525133837576,-1.70124596007879,339.616667947956));
#59512=CARTESIAN_POINT('Ctrl Pts',(82.2447478727086,-1.57208628003232,339.662241239954));
#59513=CARTESIAN_POINT('Ctrl Pts',(82.2369823616596,-1.44111132600204,339.702380376848));
#59514=CARTESIAN_POINT('Ctrl Pts',(82.2292245501373,-1.31026623401991,339.742479715672));
#59515=CARTESIAN_POINT('Ctrl Pts',(82.2214667386152,-1.17760982116692,339.777155507984));
#59516=CARTESIAN_POINT('Ctrl Pts',(82.213708927093,-1.04363138125204,339.806247663465));
#59517=CARTESIAN_POINT('Ctrl Pts',(82.20595695357,-0.909753764362079,339.835317926177));
#59518=CARTESIAN_POINT('Ctrl Pts',(82.1982049800469,-0.774556481079916,
339.858812833054));
#59519=CARTESIAN_POINT('Ctrl Pts',(82.1904530065239,-0.638543074803164,
339.876622376617));
#59520=CARTESIAN_POINT('Ctrl Pts',(82.1827043159663,-0.50258727028472,339.894424377828));
#59521=CARTESIAN_POINT('Ctrl Pts',(82.1749556254087,-0.365816416961941,
339.906545753938));
#59522=CARTESIAN_POINT('Ctrl Pts',(82.1672069348511,-0.228743103431238,
339.912927808866));
#59523=CARTESIAN_POINT('Ctrl Pts',(82.1594598564732,-0.0916983091482738,
339.919308535955));
#59524=CARTESIAN_POINT('Ctrl Pts',(82.1517127780954,0.0456484299654675,
339.91995229887));
#59525=CARTESIAN_POINT('Ctrl Pts',(82.1439656997175,0.182780960456905,339.914852407041));
#59526=CARTESIAN_POINT('Ctrl Pts',(82.1362185564117,0.319914640250844,339.909752472469));
#59527=CARTESIAN_POINT('Ctrl Pts',(82.128471413106,0.456833717237402,339.898908801666));
#59528=CARTESIAN_POINT('Ctrl Pts',(82.1207242698002,0.593023996038871,339.882366803367));
#59529=CARTESIAN_POINT('Ctrl Pts',(82.1129753847721,0.729244893306509,339.865821086076));
#59530=CARTESIAN_POINT('Ctrl Pts',(82.1052264997439,0.864736278400571,339.843574539154));
#59531=CARTESIAN_POINT('Ctrl Pts',(82.0974776147159,0.998991414537339,339.815724163216));
#59532=CARTESIAN_POINT('Ctrl Pts',(82.0897205049411,1.13338905046272,339.787844226601));
#59533=CARTESIAN_POINT('Ctrl Pts',(82.0819633951664,1.26654743292266,339.754348658879));
#59534=CARTESIAN_POINT('Ctrl Pts',(82.0742062853917,1.39797178186756,339.715385239787));
#59535=CARTESIAN_POINT('Ctrl Pts',(82.0664450304655,1.5294663597825,339.67640099989));
#59536=CARTESIAN_POINT('Ctrl Pts',(82.0586837755393,1.65922468823911,339.631943213213));
#59537=CARTESIAN_POINT('Ctrl Pts',(82.0509225206132,1.78677033947869,339.582208508619));
#59538=CARTESIAN_POINT('Ctrl Pts',(82.0431488502085,1.91452002219312,339.532394244706));
#59539=CARTESIAN_POINT('Ctrl Pts',(82.0353751798038,2.04004959650382,339.477286351766));
#59540=CARTESIAN_POINT('Ctrl Pts',(82.0276015093992,2.16290488023338,339.417128653499));
#59541=CARTESIAN_POINT('Ctrl Pts',(82.0201897052221,2.28004122094723,339.359771310561));
#59542=CARTESIAN_POINT('Ctrl Pts',(82.0127779010451,2.39474639124589,339.297823855792));
#59543=CARTESIAN_POINT('Ctrl Pts',(82.0053660968681,2.50665161159788,339.231534090678));
#59544=CARTESIAN_POINT('Ctrl Pts',(81.9975910180896,2.62404164014878,339.161995266709));
#59545=CARTESIAN_POINT('Ctrl Pts',(81.9898159393112,2.7387212852339,339.087457954934));
#59546=CARTESIAN_POINT('Ctrl Pts',(81.9820408605327,2.85023563699942,339.008159163017));
#59547=CARTESIAN_POINT('Ctrl Pts',(81.9742753494837,2.96161276325573,338.928957953312));
#59548=CARTESIAN_POINT('Ctrl Pts',(81.9665098384347,3.06983203081421,338.845007146155));
#59549=CARTESIAN_POINT('Ctrl Pts',(81.9587443273857,3.17446395032673,338.756589103239));
#59550=CARTESIAN_POINT('Ctrl Pts',(81.9509865158635,3.27899212698643,338.668258727071));
#59551=CARTESIAN_POINT('Ctrl Pts',(81.9432287043413,3.37993973733575,338.575470180319));
#59552=CARTESIAN_POINT('Ctrl Pts',(81.9354708928191,3.47690737305295,338.478548286528));
#59553=CARTESIAN_POINT('Ctrl Pts',(81.927718919296,3.57380203754919,338.381699329537));
#59554=CARTESIAN_POINT('Ctrl Pts',(81.919966945773,3.6667224135862,338.280723491965));
#59555=CARTESIAN_POINT('Ctrl Pts',(81.91221497225,3.75530349730259,338.175984682842));
#59556=CARTESIAN_POINT('Ctrl Pts',(81.9044662816924,3.84384706687744,338.071290230666));
#59557=CARTESIAN_POINT('Ctrl Pts',(81.8967175911348,3.9280547472896,337.962836274367));
#59558=CARTESIAN_POINT('Ctrl Pts',(81.8889689005771,4.0075997886505,337.851022096812));
#59559=CARTESIAN_POINT('Ctrl Pts',(81.8812218221993,4.08712828000118,337.73923118313));
#59560=CARTESIAN_POINT('Ctrl Pts',(81.8734747438215,4.16199583545949,337.624081757098));
#59561=CARTESIAN_POINT('Ctrl Pts',(81.8657276654436,4.23191750853067,337.506004242513));
#59562=CARTESIAN_POINT('Ctrl Pts',(81.8579805221378,4.30183976761282,337.387925738324));
#59563=CARTESIAN_POINT('Ctrl Pts',(81.850233378832,4.36681586246736,337.266919432964));
#59564=CARTESIAN_POINT('Ctrl Pts',(81.8424862355262,4.42660571764579,337.143442297568));
#59565=CARTESIAN_POINT('Ctrl Pts',(81.8347373504981,4.48640901485295,337.019937401891));
#59566=CARTESIAN_POINT('Ctrl Pts',(81.82698846547,4.54102358190525,336.893960922538));
#59567=CARTESIAN_POINT('Ctrl Pts',(81.8192395804419,4.59025676433914,336.765991477878));
#59568=CARTESIAN_POINT('Ctrl Pts',(81.8114824706671,4.6395422033816,336.637886205128));
#59569=CARTESIAN_POINT('Ctrl Pts',(81.8037253608924,4.68343470726242,336.507784106838));
#59570=CARTESIAN_POINT('Ctrl Pts',(81.7959682511177,4.72179079324202,336.376181226203));
#59571=CARTESIAN_POINT('Ctrl Pts',(81.7882069961915,4.76016737548755,336.244508021198));
#59572=CARTESIAN_POINT('Ctrl Pts',(81.7804457412653,4.7930015512644,336.111332815168));
#59573=CARTESIAN_POINT('Ctrl Pts',(81.7726844863391,4.82020084758153,335.97716265354));
#59574=CARTESIAN_POINT('Ctrl Pts',(81.7649108159345,4.84744365390854,335.842777863381));
#59575=CARTESIAN_POINT('Ctrl Pts',(81.7571371455298,4.86903350660446,335.707395323326));
#59576=CARTESIAN_POINT('Ctrl Pts',(81.7493634751252,4.88492965818476,335.571528911856));
#59577=CARTESIAN_POINT('Ctrl Pts',(81.7419516709481,4.90008584008457,335.441987114527));
#59578=CARTESIAN_POINT('Ctrl Pts',(81.734539866771,4.91006645320872,335.312005767375));
#59579=CARTESIAN_POINT('Ctrl Pts',(81.7271280625939,4.91488031134712,335.182029084578));
#59580=CARTESIAN_POINT('Ctrl Pts',(81.7193529838155,4.91993011101263,335.045681857377));
#59581=CARTESIAN_POINT('Ctrl Pts',(81.7115779050371,4.9193098316297,334.908908880891));
#59582=CARTESIAN_POINT('Ctrl Pts',(81.7038028262587,4.91297260017343,334.772220956967));
#59583=CARTESIAN_POINT('Ctrl Pts',(81.6960373152097,4.90664316708393,334.635701236235));
#59584=CARTESIAN_POINT('Ctrl Pts',(81.6882718041606,4.89461079762967,334.49926674654));
#59585=CARTESIAN_POINT('Ctrl Pts',(81.6805062931116,4.87688051445229,334.36343145675));
#59586=CARTESIAN_POINT('Ctrl Pts',(81.6727484815894,4.85916781090232,334.227730848045));
#59587=CARTESIAN_POINT('Ctrl Pts',(81.6649906700672,4.83576848671471,334.092628642027));
#59588=CARTESIAN_POINT('Ctrl Pts',(81.6572328585451,4.80673955017657,333.958636490332));
#59589=CARTESIAN_POINT('Ctrl Pts',(81.6494808850221,4.77773245883373,333.82474517198));
#59590=CARTESIAN_POINT('Ctrl Pts',(81.641728911499,4.74310427003886,333.691962625699));
#59591=CARTESIAN_POINT('Ctrl Pts',(81.633976937976,4.70296347812297,333.560792723079));
#59592=CARTESIAN_POINT('Ctrl Pts',(81.6262282474184,4.66283968585629,333.429678370991));
#59593=CARTESIAN_POINT('Ctrl Pts',(81.6184795568608,4.61720804794689,333.3001756772));
#59594=CARTESIAN_POINT('Ctrl Pts',(81.6107308663032,4.56622750676396,333.17277548753));
#59595=CARTESIAN_POINT('Ctrl Pts',(81.6029837879254,4.51525757250842,333.045401804533));
#59596=CARTESIAN_POINT('Ctrl Pts',(81.5952367095475,4.4589410937105,332.92013011822));
#59597=CARTESIAN_POINT('Ctrl Pts',(81.5874896311697,4.39748582202621,332.797432973193));
#59598=CARTESIAN_POINT('Ctrl Pts',(81.5797424878639,4.33603003528759,332.674734799845));
#59599=CARTESIAN_POINT('Ctrl Pts',(81.5719953445581,4.26943554480757,332.554611560308));
#59600=CARTESIAN_POINT('Ctrl Pts',(81.5642482012523,4.19795670876241,332.437512432448));
#59601=CARTESIAN_POINT('Ctrl Pts',(81.5564993162242,4.12646180275742,332.320386978219));
#59602=CARTESIAN_POINT('Ctrl Pts',(81.5487504311962,4.05008056969389,332.206287322127));
#59603=CARTESIAN_POINT('Ctrl Pts',(81.5410015461681,3.96911123358604,332.095634479284));
#59604=CARTESIAN_POINT('Ctrl Pts',(81.5332444363934,3.88805595578816,331.984864188371));
#59605=CARTESIAN_POINT('Ctrl Pts',(81.5254873266186,3.80240307813069,331.87754833481));
#59606=CARTESIAN_POINT('Ctrl Pts',(81.5177302168439,3.7124920871764,331.774076013736));
#59607=CARTESIAN_POINT('Ctrl Pts',(81.5099689619178,3.62253305066339,331.670548400362));
#59608=CARTESIAN_POINT('Ctrl Pts',(81.5022077069916,3.52831163528186,331.57086869589));
#59609=CARTESIAN_POINT('Ctrl Pts',(81.4944464520654,3.43020418390745,331.475389054207));
#59610=CARTESIAN_POINT('Ctrl Pts',(81.4866727816608,3.33193979258399,331.379756676214));
#59611=CARTESIAN_POINT('Ctrl Pts',(81.4788991112561,3.22977723451189,331.288338047811));
#59612=CARTESIAN_POINT('Ctrl Pts',(81.4711254408515,3.12412659026461,331.201445523557));
#59613=CARTESIAN_POINT('Ctrl Pts',(81.4637136366744,3.02339400892483,331.118597867213));
#59614=CARTESIAN_POINT('Ctrl Pts',(81.4563018324972,2.91949100352308,331.039864591438));
#59615=CARTESIAN_POINT('Ctrl Pts',(81.4488900283201,2.81279589288573,330.965478674308));
#59616=CARTESIAN_POINT('Ctrl Pts',(81.4411149495417,2.70087133704788,330.887446881795));
#59617=CARTESIAN_POINT('Ctrl Pts',(81.4333398707633,2.58552035443142,330.813952782353));
#59618=CARTESIAN_POINT('Ctrl Pts',(81.4255647919848,2.46714712352351,330.745312216697));
#59619=CARTESIAN_POINT('Ctrl Pts',(81.4177992809358,2.34891955841233,330.676756117626));
#59620=CARTESIAN_POINT('Ctrl Pts',(81.4100337698868,2.2276774797962,330.613041862816));
#59621=CARTESIAN_POINT('Ctrl Pts',(81.4022682588378,2.10385581310242,330.554443366667));
#59622=CARTESIAN_POINT('Ctrl Pts',(81.3945104473156,1.98015691595166,330.495902971096));
#59623=CARTESIAN_POINT('Ctrl Pts',(81.3867526357934,1.85388387166077,330.442468406169));
#59624=CARTESIAN_POINT('Ctrl Pts',(81.3789948242712,1.72549778946204,330.394368616459));
#59625=CARTESIAN_POINT('Ctrl Pts',(81.3712428507482,1.59720832186153,330.346305023365));
#59626=CARTESIAN_POINT('Ctrl Pts',(81.3634908772251,1.46680934598065,330.30356835123));
#59627=CARTESIAN_POINT('Ctrl Pts',(81.3557389037021,1.3347832906966,330.266340038683));
#59628=CARTESIAN_POINT('Ctrl Pts',(81.3479902131445,1.20281314852534,330.229127492349));
#59629=CARTESIAN_POINT('Ctrl Pts',(81.3402415225869,1.06921767288196,330.197418771702));
#59630=CARTESIAN_POINT('Ctrl Pts',(81.3324928320293,0.934495639327215,330.171345843552));
#59631=CARTESIAN_POINT('Ctrl Pts',(81.3247457536514,0.799801635816768,330.145278340094));
#59632=CARTESIAN_POINT('Ctrl Pts',(81.3169986752736,0.663981924125593,330.124844371023));
#59633=CARTESIAN_POINT('Ctrl Pts',(81.3092515968957,0.527546303432146,330.110124954538));
#59634=CARTESIAN_POINT('Ctrl Pts',(81.3015044535899,0.391109539276879,330.09540541469));
#59635=CARTESIAN_POINT('Ctrl Pts',(81.2937573102841,0.254057244442737,330.086400564882));
#59636=CARTESIAN_POINT('Ctrl Pts',(81.2860101669783,0.116904789986733,330.083139585815));
#59637=CARTESIAN_POINT('Ctrl Pts',(81.2782612819502,-0.0202784992528622,
330.079877873611));
#59638=CARTESIAN_POINT('Ctrl Pts',(81.2705123969221,-0.157561602235148,
330.082362611068));
#59639=CARTESIAN_POINT('Ctrl Pts',(81.262763511894,-0.294429092244181,330.090570850685));
#59640=CARTESIAN_POINT('Ctrl Pts',(81.2550064021193,-0.431441854821215,
330.098787802613));
#59641=CARTESIAN_POINT('Ctrl Pts',(81.2472492923446,-0.568037732425112,
330.112740368615));
#59642=CARTESIAN_POINT('Ctrl Pts',(81.2394921825698,-0.703705810998619,
330.132353628902));
#59643=CARTESIAN_POINT('Ctrl Pts',(81.2317309276437,-0.839446386255491,
330.151977369887));
#59644=CARTESIAN_POINT('Ctrl Pts',(81.2239696727174,-0.974257790605692,
330.177267760498));
#59645=CARTESIAN_POINT('Ctrl Pts',(81.2162084177913,-1.10764022960908,330.208098896654));
#59646=CARTESIAN_POINT('Ctrl Pts',(81.2084347473866,-1.24123603704555,330.23897935258));
#59647=CARTESIAN_POINT('Ctrl Pts',(81.200661076982,-1.37339793425984,330.275418161776));
#59648=CARTESIAN_POINT('Ctrl Pts',(81.1928874065773,-1.50364133750999,330.317239511716));
#59649=CARTESIAN_POINT('Ctrl Pts',(81.1854756024003,-1.62782187900365,330.357114067755));
#59650=CARTESIAN_POINT('Ctrl Pts',(81.1780637982232,-1.75025824847928,330.401881228434));
#59651=CARTESIAN_POINT('Ctrl Pts',(81.1706519940461,-1.87054979967704,330.451348935187));
#59652=CARTESIAN_POINT('Ctrl Pts',(81.1628769152677,-1.99673719812966,330.503241201605));
#59653=CARTESIAN_POINT('Ctrl Pts',(81.1551018364893,-2.12096298981029,330.560470429493));
#59654=CARTESIAN_POINT('Ctrl Pts',(81.1473267577108,-2.24274285335172,330.622867656074));
#59655=CARTESIAN_POINT('Ctrl Pts',(81.1395612466618,-2.36437285901802,330.685188098896));
#59656=CARTESIAN_POINT('Ctrl Pts',(81.1317957356128,-2.4835625807801,330.752663710189));
#59657=CARTESIAN_POINT('Ctrl Pts',(81.1240302245638,-2.59984631507018,330.825076982684));
#59658=CARTESIAN_POINT('Ctrl Pts',(81.1162724130417,-2.71601475369908,330.897418457208));
#59659=CARTESIAN_POINT('Ctrl Pts',(81.1085146015194,-2.82928260913446,330.974687644912));
#59660=CARTESIAN_POINT('Ctrl Pts',(81.1007567899973,-2.93920782433534,331.056620684252));
#59661=CARTESIAN_POINT('Ctrl Pts',(81.0930048164743,-3.04905031732592,331.138492066382));
#59662=CARTESIAN_POINT('Ctrl Pts',(81.0852528429512,-3.15555486481261,331.225020081618));
#59663=CARTESIAN_POINT('Ctrl Pts',(81.0775008694282,-3.25830782123197,331.31589723208));
#59664=CARTESIAN_POINT('Ctrl Pts',(81.0697521788706,-3.36101726171337,331.406735896014));
#59665=CARTESIAN_POINT('Ctrl Pts',(81.062003488313,-3.45997797895877,331.501919773429));
#59666=CARTESIAN_POINT('Ctrl Pts',(81.0542547977554,-3.5548090831861,331.601100848128));
#59667=CARTESIAN_POINT('Ctrl Pts',(81.0465077193775,-3.64962045701014,331.700261287376));
#59668=CARTESIAN_POINT('Ctrl Pts',(81.0387606409997,-3.74030365687123,331.803416987358));
#59669=CARTESIAN_POINT('Ctrl Pts',(81.0310135626219,-3.82651467124989,331.910183090665));
#59670=CARTESIAN_POINT('Ctrl Pts',(81.0232664193161,-3.91272640815977,332.016950088776));
#59671=CARTESIAN_POINT('Ctrl Pts',(81.0155192760103,-3.99446563926721,332.127327246455));
#59672=CARTESIAN_POINT('Ctrl Pts',(81.0077721327045,-4.07142892904662,332.240896968538));
#59673=CARTESIAN_POINT('Ctrl Pts',(81.0000232476764,-4.14840952180764,332.354492223506));
#59674=CARTESIAN_POINT('Ctrl Pts',(80.9922743626483,-4.22061181739706,332.471281147623));
#59675=CARTESIAN_POINT('Ctrl Pts',(80.9845254776202,-4.28777618588676,332.590817889357));
#59676=CARTESIAN_POINT('Ctrl Pts',(80.9767683678455,-4.35501184333107,332.710481508624));
#59677=CARTESIAN_POINT('Ctrl Pts',(80.9690112580707,-4.41719870015613,332.832898430308));
#59678=CARTESIAN_POINT('Ctrl Pts',(80.961254148296,-4.47412327309949,332.957598472482));
#59679=CARTESIAN_POINT('Ctrl Pts',(80.9534928933698,-4.53107826471449,333.082365150371));
#59680=CARTESIAN_POINT('Ctrl Pts',(80.9457316384437,-4.58276522207415,333.209417017885));
#59681=CARTESIAN_POINT('Ctrl Pts',(80.9379703835175,-4.62901955315457,333.338265653297));
#59682=CARTESIAN_POINT('Ctrl Pts',(80.9301967131129,-4.67534787609051,333.467320404534));
#59683=CARTESIAN_POINT('Ctrl Pts',(80.9224230427082,-4.71622609007985,333.598177293966));
#59684=CARTESIAN_POINT('Ctrl Pts',(80.9146493723035,-4.75153980355969,333.730333682542));
#59685=CARTESIAN_POINT('Ctrl Pts',(80.9072375681264,-4.78520965518101,333.856338159434));
#59686=CARTESIAN_POINT('Ctrl Pts',(80.8998257639494,-4.81382133962133,333.983523593974));
#59687=CARTESIAN_POINT('Ctrl Pts',(80.8924139597723,-4.83731955034643,334.111449140265));
#59688=CARTESIAN_POINT('Ctrl Pts',(80.8806823481055,-4.87451317776904,334.313933285217));
#59689=CARTESIAN_POINT('Ctrl Pts',(80.8689507364387,-4.89900138445584,334.518817720643));
#59690=CARTESIAN_POINT('Ctrl Pts',(80.8572191247719,-4.91054538093032,334.724814382055));
#59691=CARTESIAN_POINT('Ctrl Pts',(80.8520852086841,-4.91559719400601,334.814961380104));
#59692=CARTESIAN_POINT('Ctrl Pts',(80.8469512925964,-4.91817063490177,334.905321049511));
#59693=CARTESIAN_POINT('Ctrl Pts',(80.8418173765086,-4.91824819243862,334.995783357466));
#59694=CARTESIAN_POINT('',(79.0918173765422,-4.91824993919102,334.999226600024));
#59695=CARTESIAN_POINT('Ctrl Pts',(80.8418173764667,-4.91824819243925,334.995783358204));
#59696=CARTESIAN_POINT('Ctrl Pts',(80.8341698505714,-4.91836372279806,335.13053679609));
#59697=CARTESIAN_POINT('Ctrl Pts',(80.8265223246761,-4.91293699669705,335.265481447406));
#59698=CARTESIAN_POINT('Ctrl Pts',(80.8188747987808,-4.90194758541068,335.40011614862));
#59699=CARTESIAN_POINT('Ctrl Pts',(80.8112341391248,-4.89096804083545,335.534629969682));
#59700=CARTESIAN_POINT('Ctrl Pts',(80.8035934794689,-4.87443577773073,335.668833994355));
#59701=CARTESIAN_POINT('Ctrl Pts',(80.795952819813,-4.85238242166092,335.802226836036));
#59702=CARTESIAN_POINT('Ctrl Pts',(80.7883167226616,-4.83034223441963,335.935540024196));
#59703=CARTESIAN_POINT('Ctrl Pts',(80.7806806255102,-4.80278757642534,336.068042595841));
#59704=CARTESIAN_POINT('Ctrl Pts',(80.7730445283588,-4.7698018844825,336.199238527269));
#59705=CARTESIAN_POINT('Ctrl Pts',(80.7654107919207,-4.736826390126,336.330393899238));
#59706=CARTESIAN_POINT('Ctrl Pts',(80.7577770554825,-4.69842329769821,336.460243043088));
#59707=CARTESIAN_POINT('Ctrl Pts',(80.7501433190444,-4.65472700459329,336.588300845309));
#59708=CARTESIAN_POINT('Ctrl Pts',(80.742510176465,-4.61103411079685,336.716348685404));
#59709=CARTESIAN_POINT('Ctrl Pts',(80.7348770338855,-4.56204896545517,336.842605079102));
#59710=CARTESIAN_POINT('Ctrl Pts',(80.7272438913061,-4.50795544427893,336.966601325865));
#59711=CARTESIAN_POINT('Ctrl Pts',(80.719609576422,-4.4538536153722,337.090616616081));
#59712=CARTESIAN_POINT('Ctrl Pts',(80.7119752615378,-4.39464201242001,337.21237069951));
#59713=CARTESIAN_POINT('Ctrl Pts',(80.7043409466537,-4.33055189833831,337.331416590466));
#59714=CARTESIAN_POINT('Ctrl Pts',(80.6966990581132,-4.26639820337179,337.450580581431));
#59715=CARTESIAN_POINT('Ctrl Pts',(80.6890571695728,-4.19735652282173,337.56703065818));
#59716=CARTESIAN_POINT('Ctrl Pts',(80.6814152810324,-4.12370334954556,337.680345826092));
#59717=CARTESIAN_POINT('Ctrl Pts',(80.6737695893461,-4.05001352122601,337.793717387668));
#59718=CARTESIAN_POINT('Ctrl Pts',(80.6661238976599,-3.97170786410445,337.903950605303));
#59719=CARTESIAN_POINT('Ctrl Pts',(80.6584782059736,-3.88910434817903,338.010656146337));
#59720=CARTESIAN_POINT('Ctrl Pts',(80.6508204953826,-3.80637098085045,338.11752942677));
#59721=CARTESIAN_POINT('Ctrl Pts',(80.6431627847916,-3.71932651827659,338.220863644361));
#59722=CARTESIAN_POINT('Ctrl Pts',(80.6355050742006,-3.62832755438684,338.320304537324));
#59723=CARTESIAN_POINT('Ctrl Pts',(80.6283953579665,-3.54384057839536,338.412629328479));
#59724=CARTESIAN_POINT('Ctrl Pts',(80.6212856417323,-3.45594540280672,338.501598298593));
#59725=CARTESIAN_POINT('Ctrl Pts',(80.6141759254982,-3.36495254838263,338.586959354332));
#59726=CARTESIAN_POINT('Ctrl Pts',(80.6064008467198,-3.26544413086962,338.680308921478));
#59727=CARTESIAN_POINT('Ctrl Pts',(80.5986257679414,-3.16189101140127,338.769662059598));
#59728=CARTESIAN_POINT('Ctrl Pts',(80.5908506891629,-3.05464762309989,338.854647968517));
#59729=CARTESIAN_POINT('Ctrl Pts',(80.5830851781139,-2.94753620461541,338.939529296864));
#59730=CARTESIAN_POINT('Ctrl Pts',(80.5753196670649,-2.83674385622295,339.020053848591));
#59731=CARTESIAN_POINT('Ctrl Pts',(80.5675541560159,-2.7226614801003,339.095887880213));
#59732=CARTESIAN_POINT('Ctrl Pts',(80.5597963444937,-2.60869221698587,339.171646722172));
#59733=CARTESIAN_POINT('Ctrl Pts',(80.5520385329716,-2.49143974126989,339.242724084123));
#59734=CARTESIAN_POINT('Ctrl Pts',(80.5442807214494,-2.37132734738739,339.308826948722));
#59735=CARTESIAN_POINT('Ctrl Pts',(80.5365287479264,-2.25130534188994,339.37488006882));
#59736=CARTESIAN_POINT('Ctrl Pts',(80.5287767744033,-2.12842804309528,339.435965955054));
#59737=CARTESIAN_POINT('Ctrl Pts',(80.5210248008803,-2.0031466898809,339.491835526967));
#59738=CARTESIAN_POINT('Ctrl Pts',(80.5132761103227,-1.87791839339408,339.547681438083));
#59739=CARTESIAN_POINT('Ctrl Pts',(80.5055274197651,-1.75028842369582,339.598315269779));
#59740=CARTESIAN_POINT('Ctrl Pts',(80.4977787292075,-1.62073132643303,339.643534540629));
#59741=CARTESIAN_POINT('Ctrl Pts',(80.4900316508297,-1.49120118460641,339.688744403233));
#59742=CARTESIAN_POINT('Ctrl Pts',(80.4822845724519,-1.35974508155288,339.728541817041));
#59743=CARTESIAN_POINT('Ctrl Pts',(80.474537494074,-1.22685581507096,339.762773128286));
#59744=CARTESIAN_POINT('Ctrl Pts',(80.4667903507682,-1.09396543484927,339.797004726423));
#59745=CARTESIAN_POINT('Ctrl Pts',(80.4590432074624,-0.959642245759653,
339.825670031447));
#59746=CARTESIAN_POINT('Ctrl Pts',(80.4512960641566,-0.824392031065007,
339.848665882654));
#59747=CARTESIAN_POINT('Ctrl Pts',(80.4435471791285,-0.68911140925047,339.871666903818));
#59748=CARTESIAN_POINT('Ctrl Pts',(80.4357982941005,-0.552903732377097,
339.888995869321));
#59749=CARTESIAN_POINT('Ctrl Pts',(80.4280494090724,-0.416282352457188,
339.900601194296));
#59750=CARTESIAN_POINT('Ctrl Pts',(80.4202922992977,-0.279515961193069,
339.912218837282));
#59751=CARTESIAN_POINT('Ctrl Pts',(80.4125351895229,-0.14233537980844,339.918100670958));
#59752=CARTESIAN_POINT('Ctrl Pts',(80.4047780797482,-0.00525698597878473,
339.918247190473));
#59753=CARTESIAN_POINT('Ctrl Pts',(80.397016824822,0.131894658161522,339.918393788284));
#59754=CARTESIAN_POINT('Ctrl Pts',(80.3892555698958,0.268943615589085,339.912798981042));
#59755=CARTESIAN_POINT('Ctrl Pts',(80.3814943149697,0.405377163339688,339.901515318546));
#59756=CARTESIAN_POINT('Ctrl Pts',(80.373720644565,0.542028960303195,339.890213605868));
#59757=CARTESIAN_POINT('Ctrl Pts',(80.3659469741604,0.678062992298923,339.873204901333));
#59758=CARTESIAN_POINT('Ctrl Pts',(80.3581733037557,0.812974394503769,339.850593334468));
#59759=CARTESIAN_POINT('Ctrl Pts',(80.3507614995787,0.941605638478082,339.82903434148));
#59760=CARTESIAN_POINT('Ctrl Pts',(80.3433496954016,1.06921613569124,339.802382432603));
#59761=CARTESIAN_POINT('Ctrl Pts',(80.3359378912245,1.19538174061244,339.770769912363));
#59762=CARTESIAN_POINT('Ctrl Pts',(80.3281628124461,1.32773109765877,339.737607968337));
#59763=CARTESIAN_POINT('Ctrl Pts',(80.3203877336676,1.45890859258986,339.698882051086));
#59764=CARTESIAN_POINT('Ctrl Pts',(80.3126126548892,1.5884106075289,339.654689549733));
#59765=CARTESIAN_POINT('Ctrl Pts',(80.3048471438402,1.71775326199432,339.610551430066));
#59766=CARTESIAN_POINT('Ctrl Pts',(80.2970816327911,1.84542417243659,339.560960236089));
#59767=CARTESIAN_POINT('Ctrl Pts',(80.2893161217421,1.97093114724105,339.506064078033));
#59768=CARTESIAN_POINT('Ctrl Pts',(80.2815583102199,2.09631368151451,339.451222349677));
#59769=CARTESIAN_POINT('Ctrl Pts',(80.2738004986978,2.21953619410375,339.391086280345));
#59770=CARTESIAN_POINT('Ctrl Pts',(80.2660426871756,2.34012321156602,339.32585325886));
#59771=CARTESIAN_POINT('Ctrl Pts',(80.2582907136526,2.4606194834732,339.260669327292));
#59772=CARTESIAN_POINT('Ctrl Pts',(80.2505387401296,2.57848386549279,339.190396263413));
#59773=CARTESIAN_POINT('Ctrl Pts',(80.2427867666066,2.69326270930591,339.115278731892));
#59774=CARTESIAN_POINT('Ctrl Pts',(80.2350380760489,2.80799294421092,339.04019301269));
#59775=CARTESIAN_POINT('Ctrl Pts',(80.2272893854913,2.91963991351983,338.960267120005));
#59776=CARTESIAN_POINT('Ctrl Pts',(80.2195406949337,3.02777654240234,338.875790535075));
#59777=CARTESIAN_POINT('Ctrl Pts',(80.2117936165558,3.13589067255604,338.791331526205));
#59778=CARTESIAN_POINT('Ctrl Pts',(80.204046538178,3.24049560718018,338.702323948841));
#59779=CARTESIAN_POINT('Ctrl Pts',(80.1962994598002,3.34119545437707,338.609099056295));
#59780=CARTESIAN_POINT('Ctrl Pts',(80.1885523164944,3.44189614553567,338.515873382435));
#59781=CARTESIAN_POINT('Ctrl Pts',(80.1808051731885,3.5386913971573,338.418430588433));
#59782=CARTESIAN_POINT('Ctrl Pts',(80.1730580298827,3.63122075086015,338.317140172049));
#59783=CARTESIAN_POINT('Ctrl Pts',(80.1653091448545,3.72377090712654,338.215826983429));
#59784=CARTESIAN_POINT('Ctrl Pts',(80.1575602598264,3.81205299346731,338.110664739652));
#59785=CARTESIAN_POINT('Ctrl Pts',(80.1498113747983,3.89574582683509,338.002057213845));
#59786=CARTESIAN_POINT('Ctrl Pts',(80.1420542650236,3.97952749264052,337.893334410888));
#59787=CARTESIAN_POINT('Ctrl Pts',(80.1342971552488,4.05870993606958,337.781159331084));
#59788=CARTESIAN_POINT('Ctrl Pts',(80.126540045474,4.13301413191363,337.66596647539));
#59789=CARTESIAN_POINT('Ctrl Pts',(80.1187787905479,4.20735803354424,337.550712064317));
#59790=CARTESIAN_POINT('Ctrl Pts',(80.1110175356217,4.27681829550603,337.432437000976));
#59791=CARTESIAN_POINT('Ctrl Pts',(80.1032562806955,4.34116164423035,337.311600882757));
#59792=CARTESIAN_POINT('Ctrl Pts',(80.0954826102908,4.40560792134309,337.19057146613));
#59793=CARTESIAN_POINT('Ctrl Pts',(80.0877089398862,4.46492075917881,337.066973160483));
#59794=CARTESIAN_POINT('Ctrl Pts',(80.0799352694815,4.51891451115269,336.941286867878));
#59795=CARTESIAN_POINT('Ctrl Pts',(80.0725234653044,4.57039484098189,336.821451302432));
#59796=CARTESIAN_POINT('Ctrl Pts',(80.0651116611273,4.61704004454493,336.699718035696));
#59797=CARTESIAN_POINT('Ctrl Pts',(80.0576998569503,4.65873185005497,336.576515338265));
#59798=CARTESIAN_POINT('Ctrl Pts',(80.0499247781718,4.70246709514666,336.44727410963));
#59799=CARTESIAN_POINT('Ctrl Pts',(80.0421496993934,4.74088931461903,336.316007339676));
#59800=CARTESIAN_POINT('Ctrl Pts',(80.0343746206149,4.77380786853292,336.183191234261));
#59801=CARTESIAN_POINT('Ctrl Pts',(80.0266091095659,4.80668591407045,336.050538567521));
#59802=CARTESIAN_POINT('Ctrl Pts',(80.018843598517,4.83407367646886,335.916340734588));
#59803=CARTESIAN_POINT('Ctrl Pts',(80.011078087468,4.85582935165667,335.781091780836));
#59804=CARTESIAN_POINT('Ctrl Pts',(80.0033202759458,4.8775634560292,335.645976926816));
#59805=CARTESIAN_POINT('Ctrl Pts',(79.9955624644236,4.89367652444947,335.50981340942));
#59806=CARTESIAN_POINT('Ctrl Pts',(79.9878046529014,4.90407723942746,335.37310788283));
#59807=CARTESIAN_POINT('Ctrl Pts',(79.9800526793784,4.9144701275376,335.236505231483));
#59808=CARTESIAN_POINT('Ctrl Pts',(79.9723007058554,4.91915918907855,335.099361770983));
#59809=CARTESIAN_POINT('Ctrl Pts',(79.9645487323324,4.91810467265646,334.962191385972));
#59810=CARTESIAN_POINT('Ctrl Pts',(79.9568000417748,4.9170506028227,334.825079092701));
#59811=CARTESIAN_POINT('Ctrl Pts',(79.9490513512172,4.91025779591392,334.687940287647));
#59812=CARTESIAN_POINT('Ctrl Pts',(79.9413026606595,4.8977385681846,334.551290762055));
#59813=CARTESIAN_POINT('Ctrl Pts',(79.9335555822817,4.88522194518518,334.414669667539));
#59814=CARTESIAN_POINT('Ctrl Pts',(79.9258085039039,4.86698130684158,334.278538039));
#59815=CARTESIAN_POINT('Ctrl Pts',(79.9180614255261,4.8430809713081,334.143408050555));
#59816=CARTESIAN_POINT('Ctrl Pts',(79.9103142822203,4.81918043546678,334.008276929591));
#59817=CARTESIAN_POINT('Ctrl Pts',(79.9025671389144,4.78962017590249,333.874147850366));
#59818=CARTESIAN_POINT('Ctrl Pts',(79.8948199956086,4.75451584645112,333.741523886462));
#59819=CARTESIAN_POINT('Ctrl Pts',(79.8870711105805,4.71940362480125,333.608870105876));
#59820=CARTESIAN_POINT('Ctrl Pts',(79.8793222255525,4.6787449530155,333.477722491741));
#59821=CARTESIAN_POINT('Ctrl Pts',(79.8715733405244,4.63270556195336,333.348569638542));
#59822=CARTESIAN_POINT('Ctrl Pts',(79.8638162307497,4.58661730420578,333.219279701169));
#59823=CARTESIAN_POINT('Ctrl Pts',(79.856059120975,4.53513705007532,333.09198912292));
#59824=CARTESIAN_POINT('Ctrl Pts',(79.8483020112002,4.47847918413576,332.967167675443));
#59825=CARTESIAN_POINT('Ctrl Pts',(79.8405407562741,4.42179104204433,332.842279527377));
#59826=CARTESIAN_POINT('Ctrl Pts',(79.8327795013479,4.3599199513697,332.719863487828));
#59827=CARTESIAN_POINT('Ctrl Pts',(79.8250182464218,4.29312615964964,332.600364436038));
#59828=CARTESIAN_POINT('Ctrl Pts',(79.8172445760171,4.22622551963082,332.480674224709));
#59829=CARTESIAN_POINT('Ctrl Pts',(79.8094709056124,4.15438664748084,332.363910658734));
#59830=CARTESIAN_POINT('Ctrl Pts',(79.8016972352078,4.0779134799839,332.250490095987));
#59831=CARTESIAN_POINT('Ctrl Pts',(79.7942854310307,4.00500015683201,332.142349287722));
#59832=CARTESIAN_POINT('Ctrl Pts',(79.7868736268535,3.927874451917,332.037247485229));
#59833=CARTESIAN_POINT('Ctrl Pts',(79.7794618226764,3.84683250346912,331.935515907571));
#59834=CARTESIAN_POINT('Ctrl Pts',(79.771686743898,3.76181844771666,331.828798162248));
#59835=CARTESIAN_POINT('Ctrl Pts',(79.7639116651196,3.67222588803154,331.725452116884));
#59836=CARTESIAN_POINT('Ctrl Pts',(79.7561365863412,3.57835210987057,331.625895786985));
#59837=CARTESIAN_POINT('Ctrl Pts',(79.7483710752922,3.48459384936992,331.526461967488));
#59838=CARTESIAN_POINT('Ctrl Pts',(79.7406055642432,3.38656511841448,331.430808866125));
#59839=CARTESIAN_POINT('Ctrl Pts',(79.7328400531942,3.28460463197932,331.339323085264));
#59840=CARTESIAN_POINT('Ctrl Pts',(79.7250822416719,3.18274523966296,331.247928012821));
#59841=CARTESIAN_POINT('Ctrl Pts',(79.7173244301497,3.07696213885331,331.160692297505));
#59842=CARTESIAN_POINT('Ctrl Pts',(79.7095666186275,2.96763196872582,331.077966909791));
#59843=CARTESIAN_POINT('Ctrl Pts',(79.7018146451045,2.85838407301878,330.995303775554));
#59844=CARTESIAN_POINT('Ctrl Pts',(79.6940626715815,2.74559473151516,330.917144447901));
#59845=CARTESIAN_POINT('Ctrl Pts',(79.6863106980585,2.62967456901354,330.843800447093));
#59846=CARTESIAN_POINT('Ctrl Pts',(79.6785620075008,2.5138034987694,330.770487507513));
#59847=CARTESIAN_POINT('Ctrl Pts',(79.6708133169432,2.39480457428145,330.701986047323));
#59848=CARTESIAN_POINT('Ctrl Pts',(79.6630646263856,2.27311820044396,330.638564833761));
#59849=CARTESIAN_POINT('Ctrl Pts',(79.6553175480078,2.15145714447315,330.575156815512));
#59850=CARTESIAN_POINT('Ctrl Pts',(79.6475704696299,2.02711009773855,330.516827122008));
#59851=CARTESIAN_POINT('Ctrl Pts',(79.6398233912521,1.90054256462559,330.463798833545));
#59852=CARTESIAN_POINT('Ctrl Pts',(79.6320762479463,1.77397397075462,330.410770100654));
#59853=CARTESIAN_POINT('Ctrl Pts',(79.6243291046405,1.64518521389786,330.363043012468));
#59854=CARTESIAN_POINT('Ctrl Pts',(79.6165819613347,1.51466192629075,330.320792555192));
#59855=CARTESIAN_POINT('Ctrl Pts',(79.6088330763065,1.38410929427714,330.278532599116));
#59856=CARTESIAN_POINT('Ctrl Pts',(79.6010841912784,1.25182172734155,330.241751844379));
#59857=CARTESIAN_POINT('Ctrl Pts',(79.5933353062503,1.11829978148675,330.210575330875));
#59858=CARTESIAN_POINT('Ctrl Pts',(79.5855781964755,0.984636114059443,330.179365726297));
#59859=CARTESIAN_POINT('Ctrl Pts',(79.5778210867008,0.849735831737591,330.153772334456));
#59860=CARTESIAN_POINT('Ctrl Pts',(79.5700639769261,0.714109991318342,330.133869095185));
#59861=CARTESIAN_POINT('Ctrl Pts',(79.5623027219999,0.578411676786446,330.113955220259));
#59862=CARTESIAN_POINT('Ctrl Pts',(79.5545414670737,0.44198742017157,330.099737597138));
#59863=CARTESIAN_POINT('Ctrl Pts',(79.5467802121476,0.305352164793701,330.091238127801));
#59864=CARTESIAN_POINT('Ctrl Pts',(79.5390065417429,0.168498337536831,330.082725062083));
#59865=CARTESIAN_POINT('Ctrl Pts',(79.5312328713382,0.0314332280332238,
330.079948436848));
#59866=CARTESIAN_POINT('Ctrl Pts',(79.5234592009336,-0.105328561864645,
330.082877980306));
#59867=CARTESIAN_POINT('Ctrl Pts',(79.5160473967565,-0.235724057538847,
330.085671152812));
#59868=CARTESIAN_POINT('Ctrl Pts',(79.5086355925795,-0.36584354990371,330.093651187411));
#59869=CARTESIAN_POINT('Ctrl Pts',(79.5012237884025,-0.495248252394823,
330.106748296787));
#59870=CARTESIAN_POINT('Ctrl Pts',(79.4934487096241,-0.630995464833271,
330.120487334507));
#59871=CARTESIAN_POINT('Ctrl Pts',(79.4856736308456,-0.766385034037335,
330.139901154179));
#59872=CARTESIAN_POINT('Ctrl Pts',(79.4778985520672,-0.900904563630016,
330.164965974294));
#59873=CARTESIAN_POINT('Ctrl Pts',(79.4701330410182,-1.03525855837696,330.189999950553));
#59874=CARTESIAN_POINT('Ctrl Pts',(79.4623675299692,-1.16874426319003,330.220671020043));
#59875=CARTESIAN_POINT('Ctrl Pts',(79.4546020189202,-1.30085327778081,330.256903562841));
#59876=CARTESIAN_POINT('Ctrl Pts',(79.446844207398,-1.43283130589927,330.293100180968));
#59877=CARTESIAN_POINT('Ctrl Pts',(79.4390863958758,-1.56343498568158,330.33484719608));
#59878=CARTESIAN_POINT('Ctrl Pts',(79.4313285843536,-1.69216535749892,330.382017814523));
#59879=CARTESIAN_POINT('Ctrl Pts',(79.4235766108306,-1.82079885562928,330.42915293558));
#59880=CARTESIAN_POINT('Ctrl Pts',(79.4158246373075,-1.94756148624772,330.481703402131));
#59881=CARTESIAN_POINT('Ctrl Pts',(79.4080726637845,-2.07196907268009,330.539492492512));
#59882=CARTESIAN_POINT('Ctrl Pts',(79.4003239732269,-2.19632397242574,330.597257109179));
#59883=CARTESIAN_POINT('Ctrl Pts',(79.3925752826693,-2.3183254579115,330.66025577279));
#59884=CARTESIAN_POINT('Ctrl Pts',(79.3848265921117,-2.43750918867437,330.728263582847));
#59885=CARTESIAN_POINT('Ctrl Pts',(79.3770795137338,-2.55666812226654,330.796257243312));
#59886=CARTESIAN_POINT('Ctrl Pts',(79.3693324353559,-2.67301012796333,330.869257783628));
#59887=CARTESIAN_POINT('Ctrl Pts',(79.3615853569781,-2.78609570165184,330.946994472772));
#59888=CARTESIAN_POINT('Ctrl Pts',(79.3538382136723,-2.89918222310654,331.024731813426));
#59889=CARTESIAN_POINT('Ctrl Pts',(79.3460910703665,-3.00901193600733,331.107205160657));
#59890=CARTESIAN_POINT('Ctrl Pts',(79.3383439270607,-3.11517488725376,331.194100831036));
#59891=CARTESIAN_POINT('Ctrl Pts',(79.3305950420326,-3.22136170618538,331.281016037405));
#59892=CARTESIAN_POINT('Ctrl Pts',(79.3228461570044,-3.32387982065475,331.372355297805));
#59893=CARTESIAN_POINT('Ctrl Pts',(79.3150972719763,-3.42235320237136,331.467765350275));
#59894=CARTESIAN_POINT('Ctrl Pts',(79.3073401622016,-3.52093110475275,331.56327667196));
#59895=CARTESIAN_POINT('Ctrl Pts',(79.2995830524269,-3.61545541730402,331.662867144462));
#59896=CARTESIAN_POINT('Ctrl Pts',(79.2918259426521,-3.70558740028424,331.766147022304));
#59897=CARTESIAN_POINT('Ctrl Pts',(79.284064687726,-3.79576754691411,331.86948208961));
#59898=CARTESIAN_POINT('Ctrl Pts',(79.2763034327998,-3.88155044279209,331.976510185803));
#59899=CARTESIAN_POINT('Ctrl Pts',(79.2685421778737,-3.96263900470015,332.086810136478));
#59900=CARTESIAN_POINT('Ctrl Pts',(79.260768507469,-4.04385728188062,332.197286531127));
#59901=CARTESIAN_POINT('Ctrl Pts',(79.2529948370643,-4.12036600082409,332.311044914627));
#59902=CARTESIAN_POINT('Ctrl Pts',(79.2452211666597,-4.19191213713433,332.4276361655));
#59903=CARTESIAN_POINT('Ctrl Pts',(79.2378093624827,-4.26012778358583,332.538800065593));
#59904=CARTESIAN_POINT('Ctrl Pts',(79.2303975583057,-4.32383232581881,332.652538777316));
#59905=CARTESIAN_POINT('Ctrl Pts',(79.2229857541286,-4.38284699688836,332.768445549764));
#59906=CARTESIAN_POINT('Ctrl Pts',(79.2146981126954,-4.44883530708127,332.898048780879));
#59907=CARTESIAN_POINT('Ctrl Pts',(79.2064104712622,-4.50914684226371,333.030729653124));
#59908=CARTESIAN_POINT('Ctrl Pts',(79.198122829829,-4.56350325100782,333.165982240942));
#59909=CARTESIAN_POINT('Ctrl Pts',(79.1898511790019,-4.61775478167207,333.300973865388));
#59910=CARTESIAN_POINT('Ctrl Pts',(79.1815795281748,-4.6660739725485,333.438527026137));
#59911=CARTESIAN_POINT('Ctrl Pts',(79.1733078773477,-4.70822882432829,333.578112381282));
#59912=CARTESIAN_POINT('Ctrl Pts',(79.1650582852519,-4.75027125809499,333.717325492008));
#59913=CARTESIAN_POINT('Ctrl Pts',(79.1568086931562,-4.78618204660611,333.858559690968));
#59914=CARTESIAN_POINT('Ctrl Pts',(79.1485591010604,-4.81577791388594,334.001267730256));
#59915=CARTESIAN_POINT('Ctrl Pts',(79.1403231428154,-4.84532486897333,334.143739920294));
#59916=CARTESIAN_POINT('Ctrl Pts',(79.1320871845703,-4.86857763647147,334.287680792508));
#59917=CARTESIAN_POINT('Ctrl Pts',(79.1238512263252,-4.8854026029074,334.432528000686));
#59918=CARTESIAN_POINT('Ctrl Pts',(79.1156335154431,-4.90219029240967,334.577054289367));
#59919=CARTESIAN_POINT('Ctrl Pts',(79.1074158045611,-4.91257854173931,334.722482600472));
#59920=CARTESIAN_POINT('Ctrl Pts',(79.099198093679,-4.91648478403175,334.868241012131));
#59921=CARTESIAN_POINT('Ctrl Pts',(79.0967378546334,-4.91765424471822,334.911878533666));
#59922=CARTESIAN_POINT('Ctrl Pts',(79.0942776155878,-4.91824307030285,334.955545568417));
#59923=CARTESIAN_POINT('Ctrl Pts',(79.0918173765422,-4.91824993919102,334.999226600024));
#59924=CARTESIAN_POINT('',(77.341817376473,-4.91824791270454,335.004531189402));
#59925=CARTESIAN_POINT('Ctrl Pts',(79.0918173765086,-4.91824993919111,334.99922660062));
#59926=CARTESIAN_POINT('Ctrl Pts',(79.083791910814,-4.91827234595029,335.141717071739));
#59927=CARTESIAN_POINT('Ctrl Pts',(79.0757664451194,-4.91209811143813,335.284120059493));
#59928=CARTESIAN_POINT('Ctrl Pts',(79.0677409794247,-4.89977605790234,335.425884544104));
#59929=CARTESIAN_POINT('Ctrl Pts',(79.0597080005508,-4.88744246886179,335.567781744004));
#59930=CARTESIAN_POINT('Ctrl Pts',(79.0516750216769,-4.86894961308294,335.709038901325));
#59931=CARTESIAN_POINT('Ctrl Pts',(79.0436420428029,-4.84439787917671,335.849112625467));
#59932=CARTESIAN_POINT('Ctrl Pts',(79.0354008492239,-4.81920976465569,335.992817058668));
#59933=CARTESIAN_POINT('Ctrl Pts',(79.0271596556449,-4.78764450194056,336.135275487138));
#59934=CARTESIAN_POINT('Ctrl Pts',(79.0189184620659,-4.74986520391124,336.275916771256));
#59935=CARTESIAN_POINT('Ctrl Pts',(79.0108612637775,-4.71292937750462,336.41341805706));
#59936=CARTESIAN_POINT('Ctrl Pts',(79.0028040654891,-4.67005423227963,336.549182177083));
#59937=CARTESIAN_POINT('Ctrl Pts',(78.9947468672007,-4.62144139096944,336.682695020595));
#59938=CARTESIAN_POINT('Ctrl Pts',(78.9864136759764,-4.57116335534254,336.820781240652));
#59939=CARTESIAN_POINT('Ctrl Pts',(78.9780804847521,-4.51474772886055,336.95645882447));
#59940=CARTESIAN_POINT('Ctrl Pts',(78.9697472935277,-4.45246946170217,337.089186146591));
#59941=CARTESIAN_POINT('Ctrl Pts',(78.9614141023034,-4.39019119454378,337.221913468713));
#59942=CARTESIAN_POINT('Ctrl Pts',(78.9530809110791,-4.32205053731824,337.351690202885));
#59943=CARTESIAN_POINT('Ctrl Pts',(78.9447477198547,-4.2483717430536,337.478007384033));
#59944=CARTESIAN_POINT('Ctrl Pts',(78.9369726410763,-4.17962755918848,337.595864518001));
#59945=CARTESIAN_POINT('Ctrl Pts',(78.9291975622979,-4.10586669101411,337.711045098697));
#59946=CARTESIAN_POINT('Ctrl Pts',(78.9214224835194,-4.02732306754453,337.823092625495));
#59947=CARTESIAN_POINT('Ctrl Pts',(78.9136569724704,-3.9488760970039,337.935002270678));
#59948=CARTESIAN_POINT('Ctrl Pts',(78.9058914614213,-3.86565830381378,338.043786216138));
#59949=CARTESIAN_POINT('Ctrl Pts',(78.8981259503723,-3.77794914171783,338.149013074773));
#59950=CARTESIAN_POINT('Ctrl Pts',(78.8903681388501,-3.69032694351157,338.254135600672));
#59951=CARTESIAN_POINT('Ctrl Pts',(78.8826103273279,-3.59822248718326,338.355707760086));
#59952=CARTESIAN_POINT('Ctrl Pts',(78.8748525158057,-3.50195789057692,338.453327959393));
#59953=CARTESIAN_POINT('Ctrl Pts',(78.8671005422826,-3.40576573613206,338.550874696405));
#59954=CARTESIAN_POINT('Ctrl Pts',(78.8593485687596,-3.30541994613564,338.644475115667));
#59955=CARTESIAN_POINT('Ctrl Pts',(78.8515965952366,-3.20128195544908,338.733761763184));
#59956=CARTESIAN_POINT('Ctrl Pts',(78.843847904679,-3.09718806726361,338.823010597753));
#59957=CARTESIAN_POINT('Ctrl Pts',(78.8360992141213,-2.98930546872777,338.907949040231));
#59958=CARTESIAN_POINT('Ctrl Pts',(78.8283505235637,-2.87803122617068,338.988247650747));
#59959=CARTESIAN_POINT('Ctrl Pts',(78.8206034451858,-2.76678013514905,339.068529554466));
#59960=CARTESIAN_POINT('Ctrl Pts',(78.812856366808,-2.6521391204776,339.144173317798));
#59961=CARTESIAN_POINT('Ctrl Pts',(78.8051092884302,-2.53453667111569,339.214891092931));
#59962=CARTESIAN_POINT('Ctrl Pts',(78.7973621451244,-2.41693323613239,339.285609460747));
#59963=CARTESIAN_POINT('Ctrl Pts',(78.7896150018186,-2.29636865192931,339.351401556589));
#59964=CARTESIAN_POINT('Ctrl Pts',(78.7818678585128,-2.17329825733337,339.412024223321));
#59965=CARTESIAN_POINT('Ctrl Pts',(78.7741189734847,-2.05020019389978,339.472660519316));
#59966=CARTESIAN_POINT('Ctrl Pts',(78.7663700884565,-1.92459554962494,339.52812490087));
#59967=CARTESIAN_POINT('Ctrl Pts',(78.7586212034284,-1.79696163043961,339.57822148451));
#59968=CARTESIAN_POINT('Ctrl Pts',(78.7508640936537,-1.66919223929349,339.628371241181));
#59969=CARTESIAN_POINT('Ctrl Pts',(78.743106983879,-1.53938963505829,339.673141675736));
#59970=CARTESIAN_POINT('Ctrl Pts',(78.7353498741042,-1.40804888028225,339.712385957584));
#59971=CARTESIAN_POINT('Ctrl Pts',(78.7275886191781,-1.27663794120632,339.751651210322));
#59972=CARTESIAN_POINT('Ctrl Pts',(78.7198273642519,-1.14368759248009,339.785384330156));
#59973=CARTESIAN_POINT('Ctrl Pts',(78.7120661093257,-1.00970424323918,339.813489420751));
#59974=CARTESIAN_POINT('Ctrl Pts',(78.704292438921,-0.875506564304655,339.841639470333));
#59975=CARTESIAN_POINT('Ctrl Pts',(78.6965187685164,-0.740272968517659,
339.864143435795));
#59976=CARTESIAN_POINT('Ctrl Pts',(78.6887450981117,-0.604517047351342,
339.880957098968));
#59977=CARTESIAN_POINT('Ctrl Pts',(78.6813332939347,-0.475080596978326,
339.896988082074));
#59978=CARTESIAN_POINT('Ctrl Pts',(78.6739214897578,-0.345169642161097,
339.907846583985));
#59979=CARTESIAN_POINT('Ctrl Pts',(78.6665096855808,-0.215228446483766,
339.913538417304));
#59980=CARTESIAN_POINT('Ctrl Pts',(78.6587346068023,-0.0789184457292216,
339.91950922433));
#59981=CARTESIAN_POINT('Ctrl Pts',(78.6509595280239,0.0578556000153201,
339.919812957938));
#59982=CARTESIAN_POINT('Ctrl Pts',(78.6431844492455,0.194583217220188,339.914399295344));
#59983=CARTESIAN_POINT('Ctrl Pts',(78.6354189381964,0.331142582387951,339.908992294606));
#59984=CARTESIAN_POINT('Ctrl Pts',(78.6276534271474,0.467655245860287,339.897881911849));
#59985=CARTESIAN_POINT('Ctrl Pts',(78.6198879160983,0.603607216564659,339.881069697373));
#59986=CARTESIAN_POINT('Ctrl Pts',(78.6121301045761,0.73942439049408,339.864274152257));
#59987=CARTESIAN_POINT('Ctrl Pts',(78.6043722930539,0.874681592564173,339.841788073636));
#59988=CARTESIAN_POINT('Ctrl Pts',(78.5966144815317,1.00886679768246,339.813665011925));
#59989=CARTESIAN_POINT('Ctrl Pts',(78.5888625080087,1.14295102417854,339.785563113711));
#59990=CARTESIAN_POINT('Ctrl Pts',(78.5811105344857,1.27596447842093,339.751832755773));
#59991=CARTESIAN_POINT('Ctrl Pts',(78.5733585609626,1.40740256736202,339.712579025956));
#59992=CARTESIAN_POINT('Ctrl Pts',(78.565609870405,1.53878499219414,339.673341920117));
#59993=CARTESIAN_POINT('Ctrl Pts',(78.5578611798474,1.66859300492612,339.628586206426));
#59994=CARTESIAN_POINT('Ctrl Pts',(78.5501124892898,1.79633469716679,339.578467507612));
#59995=CARTESIAN_POINT('Ctrl Pts',(78.5423654109119,1.92404981168165,339.528359236411));
#59996=CARTESIAN_POINT('Ctrl Pts',(78.5346183325341,2.04969909719514,339.472890342192));
#59997=CARTESIAN_POINT('Ctrl Pts',(78.5268712541563,2.17280861637904,339.412265379495));
#59998=CARTESIAN_POINT('Ctrl Pts',(78.5191241108505,2.29591916733903,339.351639908702));
#59999=CARTESIAN_POINT('Ctrl Pts',(78.5113769675446,2.41648955885201,339.285858455923));
#60000=CARTESIAN_POINT('Ctrl Pts',(78.5036298242388,2.53406890492873,339.215172339012));
#60001=CARTESIAN_POINT('Ctrl Pts',(78.4958809392107,2.65167468533881,339.144470330361));
#60002=CARTESIAN_POINT('Ctrl Pts',(78.4881320541826,2.76628774727898,339.068861664738));
#60003=CARTESIAN_POINT('Ctrl Pts',(78.4803831691545,2.87748507052918,338.988641715093));
#60004=CARTESIAN_POINT('Ctrl Pts',(78.4726260593798,2.98880041976724,338.908336619165));
#60005=CARTESIAN_POINT('Ctrl Pts',(78.464868949605,3.09669247054324,338.823410691111));
#60006=CARTESIAN_POINT('Ctrl Pts',(78.4571118398303,3.2007698431298,338.734200781133));
#60007=CARTESIAN_POINT('Ctrl Pts',(78.4493505849041,3.3049028313366,338.64494320023));
#60008=CARTESIAN_POINT('Ctrl Pts',(78.441589329978,3.40521679385444,338.551397342363));
#60009=CARTESIAN_POINT('Ctrl Pts',(78.4338280750518,3.50135704236948,338.453937162768));
#60010=CARTESIAN_POINT('Ctrl Pts',(78.4260544046471,3.59765108394991,338.356321078648));
#60011=CARTESIAN_POINT('Ctrl Pts',(78.4182807342425,3.68975780699028,338.254778449857));
#60012=CARTESIAN_POINT('Ctrl Pts',(78.4105070638378,3.77736209367237,338.149717237434));
#60013=CARTESIAN_POINT('Ctrl Pts',(78.4030952596608,3.86088837973238,338.049546649726));
#60014=CARTESIAN_POINT('Ctrl Pts',(78.3956834554837,3.94032179758588,337.946177914735));
#60015=CARTESIAN_POINT('Ctrl Pts',(78.3882716513067,4.01542681865982,337.839987768721));
#60016=CARTESIAN_POINT('Ctrl Pts',(78.3804965725283,4.09421296054358,337.728592927327));
#60017=CARTESIAN_POINT('Ctrl Pts',(78.3727214937498,4.16848466086005,337.613741081998));
#60018=CARTESIAN_POINT('Ctrl Pts',(78.3649464149714,4.23792335558755,337.495834268269));
#60019=CARTESIAN_POINT('Ctrl Pts',(78.3571809039224,4.30727660158032,337.378072546381));
#60020=CARTESIAN_POINT('Ctrl Pts',(78.3494153928734,4.37180847898937,337.257263669674));
#60021=CARTESIAN_POINT('Ctrl Pts',(78.3416498818244,4.43124214143404,337.133840703164));
#60022=CARTESIAN_POINT('Ctrl Pts',(78.3338920703022,4.49061687522965,337.010540110884));
#60023=CARTESIAN_POINT('Ctrl Pts',(78.3261342587799,4.54490328509466,336.884630936685));
#60024=CARTESIAN_POINT('Ctrl Pts',(78.3183764472577,4.59386931655804,336.756572732592));
#60025=CARTESIAN_POINT('Ctrl Pts',(78.3106244737347,4.64279849952977,336.62861089636));
#60026=CARTESIAN_POINT('Ctrl Pts',(78.3028725002117,4.68641513433524,336.498503612843));
#60027=CARTESIAN_POINT('Ctrl Pts',(78.2951205266887,4.72453452733265,336.366732074161));
#60028=CARTESIAN_POINT('Ctrl Pts',(78.2873718361311,4.7626377767445,336.235016340805));
#60029=CARTESIAN_POINT('Ctrl Pts',(78.2796231455735,4.79524830635171,336.101638128806));
#60030=CARTESIAN_POINT('Ctrl Pts',(78.2718744550159,4.8222307827711,335.967095310812));
#60031=CARTESIAN_POINT('Ctrl Pts',(78.264127376638,4.84920764526094,335.832580485575));
#60032=CARTESIAN_POINT('Ctrl Pts',(78.2563802982602,4.87055870688119,335.696901919311));
#60033=CARTESIAN_POINT('Ctrl Pts',(78.2486332198824,4.88619950722559,335.560568852228));
#60034=CARTESIAN_POINT('Ctrl Pts',(78.2408860765765,4.90184043865498,335.424234642543));
#60035=CARTESIAN_POINT('Ctrl Pts',(78.2331389332707,4.91177096880236,335.287246309425));
#60036=CARTESIAN_POINT('Ctrl Pts',(78.2253917899649,4.91595843593344,335.150119015034));
#60037=CARTESIAN_POINT('Ctrl Pts',(78.2176429049368,4.92014684449602,335.012960891517));
#60038=CARTESIAN_POINT('Ctrl Pts',(78.2098940199087,4.91858960884494,334.875664135176));
#60039=CARTESIAN_POINT('Ctrl Pts',(78.2021451348806,4.91130619388297,334.738744315991));
#60040=CARTESIAN_POINT('Ctrl Pts',(78.1943880251059,4.90401504822911,334.601679168696));
#60041=CARTESIAN_POINT('Ctrl Pts',(78.1866309153311,4.89098560303289,334.464992148704));
#60042=CARTESIAN_POINT('Ctrl Pts',(78.1788738055564,4.87228932478686,334.32919466455));
#60043=CARTESIAN_POINT('Ctrl Pts',(78.1711125506303,4.85358305584756,334.193324614563));
#60044=CARTESIAN_POINT('Ctrl Pts',(78.1633512957041,4.82920398938614,334.058345432025));
#60045=CARTESIAN_POINT('Ctrl Pts',(78.1555900407779,4.79927465014092,333.924757750544));
#60046=CARTESIAN_POINT('Ctrl Pts',(78.1478163703733,4.76929743370681,333.790956372309));
#60047=CARTESIAN_POINT('Ctrl Pts',(78.1400426999686,4.7337523037596,333.65855132094));
#60048=CARTESIAN_POINT('Ctrl Pts',(78.132269029564,4.69281179510666,333.52802835686));
#60049=CARTESIAN_POINT('Ctrl Pts',(78.1248572253869,4.65377707698132,333.40358126816));
#60050=CARTESIAN_POINT('Ctrl Pts',(78.1174454212098,4.60983808274117,333.280845258649));
#60051=CARTESIAN_POINT('Ctrl Pts',(78.1100336170328,4.56118415991932,333.160222262935));
#60052=CARTESIAN_POINT('Ctrl Pts',(78.1022585382543,4.51014556340726,333.033687174883));
#60053=CARTESIAN_POINT('Ctrl Pts',(78.0944834594759,4.4537568751639,332.909077593865));
#60054=CARTESIAN_POINT('Ctrl Pts',(78.0867083806975,4.39218378217622,332.786878971658));
#60055=CARTESIAN_POINT('Ctrl Pts',(78.0789428696485,4.33068645879943,332.664830722636));
#60056=CARTESIAN_POINT('Ctrl Pts',(78.0711773585994,4.26401759873661,332.545187874998));
#60057=CARTESIAN_POINT('Ctrl Pts',(78.0634118475504,4.19239155813625,332.428417591099));
#60058=CARTESIAN_POINT('Ctrl Pts',(78.0556540360282,4.12083653496359,332.311763085277));
#60059=CARTESIAN_POINT('Ctrl Pts',(78.0478962245061,4.04433431555666,332.197975806246));
#60060=CARTESIAN_POINT('Ctrl Pts',(78.0401384129839,3.9631457690288,332.087499583531));
#60061=CARTESIAN_POINT('Ctrl Pts',(78.0323864394609,3.88201831945728,331.977106497679));
#60062=CARTESIAN_POINT('Ctrl Pts',(78.0246344659379,3.79621179284604,331.870019822286));
#60063=CARTESIAN_POINT('Ctrl Pts',(78.016882492415,3.70603088558811,331.766655270843));
#60064=CARTESIAN_POINT('Ctrl Pts',(78.0091338018573,3.61588816999759,331.663334494349));
#60065=CARTESIAN_POINT('Ctrl Pts',(78.0013851112997,3.52137501479023,331.563733000534));
#60066=CARTESIAN_POINT('Ctrl Pts',(77.9936364207421,3.42283685503905,331.468234021585));
#60067=CARTESIAN_POINT('Ctrl Pts',(77.9858893423643,3.32431919697509,331.372754911997));
#60068=CARTESIAN_POINT('Ctrl Pts',(77.9781422639865,3.22177848059466,331.281376891336));
#60069=CARTESIAN_POINT('Ctrl Pts',(77.9703951856087,3.11559723048165,331.194446563256));
#60070=CARTESIAN_POINT('Ctrl Pts',(77.9626480423028,3.00941509046734,331.107515506616));
#60071=CARTESIAN_POINT('Ctrl Pts',(77.954900898997,2.89959265830718,331.025032464518));
#60072=CARTESIAN_POINT('Ctrl Pts',(77.9471537556912,2.78654546971325,330.947303686714));
#60073=CARTESIAN_POINT('Ctrl Pts',(77.9394048706632,2.67347286571204,330.869557433832));
#60074=CARTESIAN_POINT('Ctrl Pts',(77.9316559856351,2.55717438464273,330.796567793571));
#60075=CARTESIAN_POINT('Ctrl Pts',(77.9239071006071,2.43809411387698,330.728597401979));
#60076=CARTESIAN_POINT('Ctrl Pts',(77.9161499908323,2.31888745008079,330.660554865911));
#60077=CARTESIAN_POINT('Ctrl Pts',(77.9083928810576,2.19689343845477,330.59754241473));
#60078=CARTESIAN_POINT('Ctrl Pts',(77.9006357712829,2.07258080796605,330.539776703241));
#60079=CARTESIAN_POINT('Ctrl Pts',(77.8928745163567,1.94820174878226,330.481980123602));
#60080=CARTESIAN_POINT('Ctrl Pts',(77.8851132614305,1.82150196279881,330.429436019919));
#60081=CARTESIAN_POINT('Ctrl Pts',(77.8773520065044,1.69296874866233,330.382312280096));
#60082=CARTESIAN_POINT('Ctrl Pts',(77.8695783360997,1.56422992327228,330.335113157647));
#60083=CARTESIAN_POINT('Ctrl Pts',(77.861804665695,1.43365218144478,330.293351845045));
#60084=CARTESIAN_POINT('Ctrl Pts',(77.8540309952904,1.30173737796668,330.257146126929));
#60085=CARTESIAN_POINT('Ctrl Pts',(77.8466191911132,1.1759632403262,330.222625793701));
#60086=CARTESIAN_POINT('Ctrl Pts',(77.8392073869361,1.04897400046618,330.193155534017));
#60087=CARTESIAN_POINT('Ctrl Pts',(77.8317955827589,0.921210120589533,330.168793631377));
#60088=CARTESIAN_POINT('Ctrl Pts',(77.8240205039805,0.787184152372231,330.143237679318));
#60089=CARTESIAN_POINT('Ctrl Pts',(77.8162454252021,0.651882142474197,330.123222735876));
#60090=CARTESIAN_POINT('Ctrl Pts',(77.8084703464236,0.515801980388661,330.108872177143));
#60091=CARTESIAN_POINT('Ctrl Pts',(77.8007048353746,0.379889273606136,330.094539277685));
#60092=CARTESIAN_POINT('Ctrl Pts',(77.7929393243256,0.243200704920283,330.085856934468));
#60093=CARTESIAN_POINT('Ctrl Pts',(77.7851738132766,0.106245121535196,330.082897699188));
#60094=CARTESIAN_POINT('Ctrl Pts',(77.7774160017544,-0.0305746699905079,
330.079941397999));
#60095=CARTESIAN_POINT('Ctrl Pts',(77.7696581902322,-0.167660561090477,
330.082696920605));
#60096=CARTESIAN_POINT('Ctrl Pts',(77.76190037871,-0.304498154801893,330.091185078227));
#60097=CARTESIAN_POINT('Ctrl Pts',(77.754148405187,-0.441232773885044,330.099666848241));
#60098=CARTESIAN_POINT('Ctrl Pts',(77.7463964316639,-0.577719078945123,
330.113872642383));
#60099=CARTESIAN_POINT('Ctrl Pts',(77.7386444581408,-0.713442598936831,
330.13377120138));
#60100=CARTESIAN_POINT('Ctrl Pts',(77.7308957675832,-0.849108639936781,
330.153661333324));
#60101=CARTESIAN_POINT('Ctrl Pts',(77.7231470770256,-0.984012152436957,
330.179239378452));
#60102=CARTESIAN_POINT('Ctrl Pts',(77.715398386468,-1.11764393357606,330.210422241967));
#60103=CARTESIAN_POINT('Ctrl Pts',(77.7076513080902,-1.25124791150698,330.241598617627));
#60104=CARTESIAN_POINT('Ctrl Pts',(77.6999042297123,-1.38358030396448,330.278377403392));
#60105=CARTESIAN_POINT('Ctrl Pts',(77.6921571513345,-1.51414263853909,330.320624493305));
#60106=CARTESIAN_POINT('Ctrl Pts',(77.6844100080287,-1.64470606735174,330.362871937289));
#60107=CARTESIAN_POINT('Ctrl Pts',(77.6766628647228,-1.77349903680248,330.410587656496));
#60108=CARTESIAN_POINT('Ctrl Pts',(77.668915721417,-1.90003914472251,330.463587947395));
#60109=CARTESIAN_POINT('Ctrl Pts',(77.6611668363889,-2.0266077015454,330.516600153884));
#60110=CARTESIAN_POINT('Ctrl Pts',(77.6534179513608,-2.15092202851932,330.574899145245));
#60111=CARTESIAN_POINT('Ctrl Pts',(77.6456690663327,-2.27252094822998,330.638253606369));
#60112=CARTESIAN_POINT('Ctrl Pts',(77.637911956558,-2.3942489342903,330.701675312571));
#60113=CARTESIAN_POINT('Ctrl Pts',(77.6301548467833,-2.51325540850563,330.770163026588));
#60114=CARTESIAN_POINT('Ctrl Pts',(77.6223977370085,-2.62910452508903,330.843439828577));
#60115=CARTESIAN_POINT('Ctrl Pts',(77.6146364820824,-2.74501554773595,330.916755787346));
#60116=CARTESIAN_POINT('Ctrl Pts',(77.6068752271562,-2.85776552972986,330.994865710918));
#60117=CARTESIAN_POINT('Ctrl Pts',(77.5991139722301,-2.96694958529134,331.077450673243));
#60118=CARTESIAN_POINT('Ctrl Pts',(77.5913403018254,-3.07630829975895,331.160167744594));
#60119=CARTESIAN_POINT('Ctrl Pts',(77.5835666314207,-3.18208938711603,331.247373910939));
#60120=CARTESIAN_POINT('Ctrl Pts',(77.5757929610161,-3.28392221732683,331.338710891906));
#60121=CARTESIAN_POINT('Ctrl Pts',(77.568381156839,-3.38101470479113,331.425796114435));
#60122=CARTESIAN_POINT('Ctrl Pts',(77.560969352662,-3.47451803920769,331.51663602691));
#60123=CARTESIAN_POINT('Ctrl Pts',(77.5535575484849,-3.56414484936622,331.610891775815));
#60124=CARTESIAN_POINT('Ctrl Pts',(77.5458780966147,-3.6570081736601,331.708551194483));
#60125=CARTESIAN_POINT('Ctrl Pts',(77.5381986447444,-3.74601944247178,331.81020378446));
#60126=CARTESIAN_POINT('Ctrl Pts',(77.5305191928742,-3.83080915142889,331.915509068286));
#60127=CARTESIAN_POINT('Ctrl Pts',(77.5226566171923,-3.91762075139546,332.023325456456));
#60128=CARTESIAN_POINT('Ctrl Pts',(77.5147940415104,-4.00000657169024,332.134970702031));
#60129=CARTESIAN_POINT('Ctrl Pts',(77.5069314658285,-4.07760827444734,332.250037487045));
#60130=CARTESIAN_POINT('Ctrl Pts',(77.4992708826123,-4.15321636087354,332.362148163963));
#60131=CARTESIAN_POINT('Ctrl Pts',(77.4916102993961,-4.22428287453687,332.477506381221));
#60132=CARTESIAN_POINT('Ctrl Pts',(77.4839497161799,-4.29051616916872,332.595700920309));
#60133=CARTESIAN_POINT('Ctrl Pts',(77.4762941438879,-4.35670613942,332.71381814624));
#60134=CARTESIAN_POINT('Ctrl Pts',(77.468638571596,-4.41806898185686,332.834767656018));
#60135=CARTESIAN_POINT('Ctrl Pts',(77.460982999304,-4.47435662834311,332.958109742199));
#60136=CARTESIAN_POINT('Ctrl Pts',(77.4533306794578,-4.53062036119993,333.081399426883));
#60137=CARTESIAN_POINT('Ctrl Pts',(77.4456783596117,-4.58181302090117,333.207079301473));
#60138=CARTESIAN_POINT('Ctrl Pts',(77.4380260397656,-4.62773298058989,333.334686058768));
#60139=CARTESIAN_POINT('Ctrl Pts',(77.4300086511608,-4.6758436410093,333.468380543891));
#60140=CARTESIAN_POINT('Ctrl Pts',(77.4219912625561,-4.71816590548938,333.604189874275));
#60141=CARTESIAN_POINT('Ctrl Pts',(77.4139738739513,-4.7545252176284,333.741559291251));
#60142=CARTESIAN_POINT('Ctrl Pts',(77.4063206178141,-4.78923316837023,333.872689686118));
#60143=CARTESIAN_POINT('Ctrl Pts',(77.3986673616769,-4.81850782164082,334.005241152015));
#60144=CARTESIAN_POINT('Ctrl Pts',(77.3910141055398,-4.8422491117242,334.138718047033));
#60145=CARTESIAN_POINT('Ctrl Pts',(77.3833592324799,-4.8659954176897,334.272223142051));
#60146=CARTESIAN_POINT('Ctrl Pts',(77.37570435942,-4.88420597349974,334.406653658603));
#60147=CARTESIAN_POINT('Ctrl Pts',(77.3680494863601,-4.89683235347569,334.541506854518));
#60148=CARTESIAN_POINT('Ctrl Pts',(77.3603889927685,-4.90946800427409,334.676459065356));
#60149=CARTESIAN_POINT('Ctrl Pts',(77.3527284991769,-4.91651127301378,334.811834174747));
#60150=CARTESIAN_POINT('Ctrl Pts',(77.3450680055853,-4.91796579558135,334.947127549784));
#60151=CARTESIAN_POINT('Ctrl Pts',(77.3439844625598,-4.91817153138216,334.966264200859));
#60152=CARTESIAN_POINT('Ctrl Pts',(77.3429009195342,-4.91826553901394,334.985399221222));
#60153=CARTESIAN_POINT('Ctrl Pts',(77.3418173765086,-4.91824791270512,335.004531188772));
#60154=CARTESIAN_POINT('',(75.5918173764532,-4.91824976747205,334.998487630632));
#60155=CARTESIAN_POINT('Ctrl Pts',(77.3418173764729,-4.91824791270454,335.004531189402));
#60156=CARTESIAN_POINT('Ctrl Pts',(77.3316909005339,-4.91808318235906,335.183332957754));
#60157=CARTESIAN_POINT('Ctrl Pts',(77.3215644245949,-4.9081646217589,335.361701101329));
#60158=CARTESIAN_POINT('Ctrl Pts',(77.3114379486558,-4.88865408756588,335.538743236269));
#60159=CARTESIAN_POINT('Ctrl Pts',(77.3010502676183,-4.86864029330125,335.720352044608));
#60160=CARTESIAN_POINT('Ctrl Pts',(77.2906625865807,-4.83853326650481,335.900565920531));
#60161=CARTESIAN_POINT('Ctrl Pts',(77.2802749055432,-4.79855541263399,336.078447501912));
#60162=CARTESIAN_POINT('Ctrl Pts',(77.2786231084325,-4.7921983341602,336.106733341756));
#60163=CARTESIAN_POINT('Ctrl Pts',(77.2769713113217,-4.78559176117621,336.13496025278));
#60164=CARTESIAN_POINT('Ctrl Pts',(77.275319514211,-4.77873669775026,336.163124514433));
#60165=CARTESIAN_POINT('Ctrl Pts',(77.2675444354326,-4.74646962461989,336.295694883799));
#60166=CARTESIAN_POINT('Ctrl Pts',(77.2597693566541,-4.70863078847159,336.427131006392));
#60167=CARTESIAN_POINT('Ctrl Pts',(77.2519942778757,-4.66531417390901,336.556928617896));
#60168=CARTESIAN_POINT('Ctrl Pts',(77.2442287668267,-4.62205086319838,336.686566505175));
#60169=CARTESIAN_POINT('Ctrl Pts',(77.2364632557777,-4.57332330879617,336.81456952598));
#60170=CARTESIAN_POINT('Ctrl Pts',(77.2286977447287,-4.51927629244884,336.940444499338));
#60171=CARTESIAN_POINT('Ctrl Pts',(77.2209399332065,-4.46528286387542,337.066194667293));
#60172=CARTESIAN_POINT('Ctrl Pts',(77.2131821216842,-4.40598062265845,337.189820629899));
#60173=CARTESIAN_POINT('Ctrl Pts',(77.205424310162,-4.34156374095501,337.310845591061));
#60174=CARTESIAN_POINT('Ctrl Pts',(77.197672336639,-4.27719533499791,337.431779477101));
#60175=CARTESIAN_POINT('Ctrl Pts',(77.189920363116,-4.20772013257298,337.550115914026));
#60176=CARTESIAN_POINT('Ctrl Pts',(77.1821683895929,-4.13337972805088,337.665399610985));
#60177=CARTESIAN_POINT('Ctrl Pts',(77.1744196990353,-4.05907080673423,337.780634485229));
#60178=CARTESIAN_POINT('Ctrl Pts',(77.1666710084777,-3.97990099273244,337.892818863056));
#60179=CARTESIAN_POINT('Ctrl Pts',(77.1589223179201,-3.89615687548517,338.001523723729));
#60180=CARTESIAN_POINT('Ctrl Pts',(77.1511752395422,-3.812430181901,338.110205967448));
#60181=CARTESIAN_POINT('Ctrl Pts',(77.1434281611644,-3.72413131650783,338.215409824536));
#60182=CARTESIAN_POINT('Ctrl Pts',(77.1356810827865,-3.63158885052608,338.316737174278));
#60183=CARTESIAN_POINT('Ctrl Pts',(77.1279339394807,-3.53904560894933,338.41806537324));
#60184=CARTESIAN_POINT('Ctrl Pts',(77.1201867961749,-3.44225895944124,338.515516711437));
#60185=CARTESIAN_POINT('Ctrl Pts',(77.1124396528691,-3.34159595617698,338.608728242492));
#60186=CARTESIAN_POINT('Ctrl Pts',(77.104690767841,-3.24091032173253,338.701960729478));
#60187=CARTESIAN_POINT('Ctrl Pts',(77.0969418828128,-3.13634688611585,338.790951247045));
#60188=CARTESIAN_POINT('Ctrl Pts',(77.0891929977847,-3.02830724341881,338.875375891698));
#60189=CARTESIAN_POINT('Ctrl Pts',(77.08143588801,-2.92015292632868,338.959890145542));
#60190=CARTESIAN_POINT('Ctrl Pts',(77.0736787782353,-2.80851534015112,339.039828604552));
#60191=CARTESIAN_POINT('Ctrl Pts',(77.0659216684606,-2.6938270909141,339.114909314524));
#60192=CARTESIAN_POINT('Ctrl Pts',(77.0581604135344,-2.57907755594371,339.190030145227));
#60193=CARTESIAN_POINT('Ctrl Pts',(77.0503991586082,-2.46127444517347,339.260287854362));
#60194=CARTESIAN_POINT('Ctrl Pts',(77.042637903682,-2.34087576957709,339.325446068778));
#60195=CARTESIAN_POINT('Ctrl Pts',(77.0348642332773,-2.22028449533759,339.390708515102));
#60196=CARTESIAN_POINT('Ctrl Pts',(77.0270905628726,-2.09708971066319,339.450854993968));
#60197=CARTESIAN_POINT('Ctrl Pts',(77.019316892468,-1.97177105246695,339.505696614193));
#60198=CARTESIAN_POINT('Ctrl Pts',(77.011905088291,-1.85228600796204,339.557985343802));
#60199=CARTESIAN_POINT('Ctrl Pts',(77.0044932841141,-1.73087064075181,339.605451877806));
#60200=CARTESIAN_POINT('Ctrl Pts',(76.9970814799371,-1.60795241264849,339.647975053844));
#60201=CARTESIAN_POINT('Ctrl Pts',(76.9893064011587,-1.47900959602892,339.692582417411));
#60202=CARTESIAN_POINT('Ctrl Pts',(76.9815313223802,-1.34800539104188,339.731890560576));
#60203=CARTESIAN_POINT('Ctrl Pts',(76.9737562436018,-1.21541470477148,339.765705630641));
#60204=CARTESIAN_POINT('Ctrl Pts',(76.9659907325528,-1.08298717978167,339.79947908911));
#60205=CARTESIAN_POINT('Ctrl Pts',(76.9582252215038,-0.948977433088734,
339.827772828425));
#60206=CARTESIAN_POINT('Ctrl Pts',(76.9504597104548,-0.813878540804875,
339.850441710125));
#60207=CARTESIAN_POINT('Ctrl Pts',(76.9427018989326,-0.678913599465953,
339.873088115562));
#60208=CARTESIAN_POINT('Ctrl Pts',(76.9349440874104,-0.542862044582386,
339.890120697787));
#60209=CARTESIAN_POINT('Ctrl Pts',(76.9271862758882,-0.406229901857792,
339.901444718584));
#60210=CARTESIAN_POINT('Ctrl Pts',(76.9194343023652,-0.269700579153639,
339.912760217697));
#60211=CARTESIAN_POINT('Ctrl Pts',(76.9116823288422,-0.132591926228203,
339.918375673953));
#60212=CARTESIAN_POINT('Ctrl Pts',(76.9039303553192,0.00458245255235774,
339.918247865209));
#60213=CARTESIAN_POINT('Ctrl Pts',(76.8961816647616,0.141698737902157,339.918120110592));
#60214=CARTESIAN_POINT('Ctrl Pts',(76.888432974204,0.278880303684706,339.912253928964));
#60215=CARTESIAN_POINT('Ctrl Pts',(76.8806842836463,0.415611287219802,339.900658151762));
#60216=CARTESIAN_POINT('Ctrl Pts',(76.8729372052685,0.55231382273168,339.889064787159));
#60217=CARTESIAN_POINT('Ctrl Pts',(76.8651901268907,0.688565573234652,339.871744231143));
#60218=CARTESIAN_POINT('Ctrl Pts',(76.8574430485128,0.823853941784865,339.848757340299));
#60219=CARTESIAN_POINT('Ctrl Pts',(76.849695905207,0.959143444181912,339.825770256804));
#60220=CARTESIAN_POINT('Ctrl Pts',(76.8419487619013,1.09346916317045,339.797116809235));
#60221=CARTESIAN_POINT('Ctrl Pts',(76.8342016185955,1.22632725532357,339.76290925017));
#60222=CARTESIAN_POINT('Ctrl Pts',(76.8264527335674,1.35921521679645,339.728694000519));
#60223=CARTESIAN_POINT('Ctrl Pts',(76.8187038485393,1.49063451640824,339.688922252076));
#60224=CARTESIAN_POINT('Ctrl Pts',(76.8109549635112,1.62009545119503,339.643756431114));
#60225=CARTESIAN_POINT('Ctrl Pts',(76.8031978537365,1.74969379715558,339.598542670684));
#60226=CARTESIAN_POINT('Ctrl Pts',(76.7954407439617,1.87732925639334,339.547923529822));
#60227=CARTESIAN_POINT('Ctrl Pts',(76.787683634187,2.00253061965779,339.492110214569));
#60228=CARTESIAN_POINT('Ctrl Pts',(76.7799223792608,2.1277988865277,339.436267074464));
#60229=CARTESIAN_POINT('Ctrl Pts',(76.7721611243347,2.25063011580118,339.375224403198));
#60230=CARTESIAN_POINT('Ctrl Pts',(76.7643998694085,2.37057768023263,339.309239436894));
#60231=CARTESIAN_POINT('Ctrl Pts',(76.7566261990038,2.49071712167627,339.243148916148));
#60232=CARTESIAN_POINT('Ctrl Pts',(76.7488525285992,2.60796334582652,339.172100504389));
#60233=CARTESIAN_POINT('Ctrl Pts',(76.7410788581945,2.72189795100158,339.096395318671));
#60234=CARTESIAN_POINT('Ctrl Pts',(76.7336670540174,2.83052887289558,339.024214227562));
#60235=CARTESIAN_POINT('Ctrl Pts',(76.7262552498402,2.93614931600617,338.947800320168));
#60236=CARTESIAN_POINT('Ctrl Pts',(76.7188434456631,3.03842606820501,338.867447490342));
#60237=CARTESIAN_POINT('Ctrl Pts',(76.7110683668846,3.145715708695,338.783156328968));
#60238=CARTESIAN_POINT('Ctrl Pts',(76.7032932881062,3.24966465722322,338.69426398991));
#60239=CARTESIAN_POINT('Ctrl Pts',(76.6955182093278,3.34985289944657,338.601064927847));
#60240=CARTESIAN_POINT('Ctrl Pts',(76.6877526982787,3.44991785365957,338.507980553163));
#60241=CARTESIAN_POINT('Ctrl Pts',(76.6799871872297,3.54623102608384,338.410600264035));
#60242=CARTESIAN_POINT('Ctrl Pts',(76.6722216761807,3.63840353491179,338.309260155932));
#60243=CARTESIAN_POINT('Ctrl Pts',(76.6644638646585,3.73048465442894,338.208020526842));
#60244=CARTESIAN_POINT('Ctrl Pts',(76.6567060531363,3.8184330191803,338.102829179379));
#60245=CARTESIAN_POINT('Ctrl Pts',(76.6489482416141,3.90189512223501,337.994060373068));
#60246=CARTESIAN_POINT('Ctrl Pts',(76.6411962680911,3.98529441741033,337.885373418734));
#60247=CARTESIAN_POINT('Ctrl Pts',(76.6334442945681,4.0642139337672,337.773114672999));
#60248=CARTESIAN_POINT('Ctrl Pts',(76.6256923210451,4.13833938409002,337.65769264675));
#60249=CARTESIAN_POINT('Ctrl Pts',(76.6179436304874,4.21243344224068,337.542319501798));
#60250=CARTESIAN_POINT('Ctrl Pts',(76.6101949399298,4.28173726168209,337.423786069011));
#60251=CARTESIAN_POINT('Ctrl Pts',(76.6024462493722,4.34597910606102,337.302530927519));
#60252=CARTESIAN_POINT('Ctrl Pts',(76.5946991709943,4.41020758438767,337.181301014172));
#60253=CARTESIAN_POINT('Ctrl Pts',(76.5869520926165,4.4693759996366,337.057350863656));
#60254=CARTESIAN_POINT('Ctrl Pts',(76.5792050142387,4.52325813178996,336.931144462669));
#60255=CARTESIAN_POINT('Ctrl Pts',(76.5714578709329,4.57714071552746,336.80493700395));
#60256=CARTESIAN_POINT('Ctrl Pts',(76.563710727627,4.62573677432516,336.676473616525));
#60257=CARTESIAN_POINT('Ctrl Pts',(76.5559635843212,4.66886804518057,336.54623873939));
#60258=CARTESIAN_POINT('Ctrl Pts',(76.5482146992931,4.71200901286134,336.415974582691));
#60259=CARTESIAN_POINT('Ctrl Pts',(76.540465814265,4.74968262496021,336.283938514755));
#60260=CARTESIAN_POINT('Ctrl Pts',(76.5327169292369,4.78176046282318,336.150630235428));
#60261=CARTESIAN_POINT('Ctrl Pts',(76.5249598194622,4.81387234843471,336.017180461316));
#60262=CARTESIAN_POINT('Ctrl Pts',(76.5172027096875,4.84037650368658,335.882456159014));
#60263=CARTESIAN_POINT('Ctrl Pts',(76.5094455999127,4.86119553787986,335.74696787414));
#60264=CARTESIAN_POINT('Ctrl Pts',(76.5016843449866,4.88202569709936,335.611407188658));
#60265=CARTESIAN_POINT('Ctrl Pts',(76.4939230900604,4.89716463875778,335.475082095423));
#60266=CARTESIAN_POINT('Ctrl Pts',(76.4861618351342,4.90658698256869,335.33850737804));
#60267=CARTESIAN_POINT('Ctrl Pts',(76.4783881647296,4.91602439905897,335.201714185619));
#60268=CARTESIAN_POINT('Ctrl Pts',(76.4706144943249,4.91972693333389,335.064670962032));
#60269=CARTESIAN_POINT('Ctrl Pts',(76.4628408239202,4.91772137999068,334.927892501898));
#60270=CARTESIAN_POINT('Ctrl Pts',(76.4554290197432,4.91580918563812,334.797481111991));
#60271=CARTESIAN_POINT('Ctrl Pts',(76.4480172155662,4.90870838295846,334.667310678148));
#60272=CARTESIAN_POINT('Ctrl Pts',(76.4406054113892,4.89648579335925,334.537820448385));
#60273=CARTESIAN_POINT('Ctrl Pts',(76.4328303326108,4.88366413823442,334.401983516728));
#60274=CARTESIAN_POINT('Ctrl Pts',(76.4250552538323,4.86516541452339,334.266465882951));
#60275=CARTESIAN_POINT('Ctrl Pts',(76.4172801750539,4.84100994158732,334.1317800924));
#60276=CARTESIAN_POINT('Ctrl Pts',(76.4095146640049,4.8168841934985,333.997260041289));
#60277=CARTESIAN_POINT('Ctrl Pts',(76.4017491529559,4.78711561490042,333.863570177719));
#60278=CARTESIAN_POINT('Ctrl Pts',(76.3939836419069,4.75177638938504,333.731219401243));
#60279=CARTESIAN_POINT('Ctrl Pts',(76.3862258303847,4.71647220281465,333.598999850947));
#60280=CARTESIAN_POINT('Ctrl Pts',(76.3784680188625,4.67560846121725,333.468117120741));
#60281=CARTESIAN_POINT('Ctrl Pts',(76.3707102073403,4.62930858452745,333.339071015449));
#60282=CARTESIAN_POINT('Ctrl Pts',(76.3629582338173,4.58304354996315,333.210122021444));
#60283=CARTESIAN_POINT('Ctrl Pts',(76.3552062602943,4.53135065444095,333.083007267743));
#60284=CARTESIAN_POINT('Ctrl Pts',(76.3474542867713,4.4744033446347,332.958212113852));
#60285=CARTESIAN_POINT('Ctrl Pts',(76.3397055962137,4.41748015204792,332.833469810782));
#60286=CARTESIAN_POINT('Ctrl Pts',(76.3319569056561,4.35530713296958,332.711045508554));
#60287=CARTESIAN_POINT('Ctrl Pts',(76.3242082150985,4.28810604581396,332.591405056396));
#60288=CARTESIAN_POINT('Ctrl Pts',(76.3164611367206,4.22091894040584,332.471789496434));
#60289=CARTESIAN_POINT('Ctrl Pts',(76.3087140583428,4.14870603905123,332.354956975046));
#60290=CARTESIAN_POINT('Ctrl Pts',(76.300966979965,4.07173509742965,332.241348815298));
#60291=CARTESIAN_POINT('Ctrl Pts',(76.2932198366592,3.99476351071744,332.127739703403));
#60292=CARTESIAN_POINT('Ctrl Pts',(76.2854726933534,3.91303402344244,332.017355330645));
#60293=CARTESIAN_POINT('Ctrl Pts',(76.2777255500476,3.8268575423528,331.910607759925));
#60294=CARTESIAN_POINT('Ctrl Pts',(76.2699766650195,3.74066168696069,331.803836190084));
#60295=CARTESIAN_POINT('Ctrl Pts',(76.2622277799914,3.65001709378535,331.70070335335));
#60296=CARTESIAN_POINT('Ctrl Pts',(76.2544788949634,3.55527447638604,331.60158765597));
#60297=CARTESIAN_POINT('Ctrl Pts',(76.2467217851886,3.46043129819367,331.502366756164));
#60298=CARTESIAN_POINT('Ctrl Pts',(76.2389646754139,3.36148167738588,331.407171796116));
#60299=CARTESIAN_POINT('Ctrl Pts',(76.2312075656392,3.25881306211745,331.316344140847));
#60300=CARTESIAN_POINT('Ctrl Pts',(76.223446310713,3.15608958402373,331.225467950183));
#60301=CARTESIAN_POINT('Ctrl Pts',(76.2156850557868,3.04964345475786,331.138963960885));
#60302=CARTESIAN_POINT('Ctrl Pts',(76.2079238008606,2.93989383210682,331.057132094726));
#60303=CARTESIAN_POINT('Ctrl Pts',(76.200150130456,2.82996864582694,330.97516932425));
#60304=CARTESIAN_POINT('Ctrl Pts',(76.1923764600514,2.71672972917205,330.897893832367));
#60305=CARTESIAN_POINT('Ctrl Pts',(76.1846027896467,2.60062448401203,330.825561671835));
#60306=CARTESIAN_POINT('Ctrl Pts',(76.1771909854696,2.48992396594666,330.756596590776));
#60307=CARTESIAN_POINT('Ctrl Pts',(76.1697791812924,2.37661821928833,330.692125116308));
#60308=CARTESIAN_POINT('Ctrl Pts',(76.1623673771153,2.26111277796105,330.632328759185));
#60309=CARTESIAN_POINT('Ctrl Pts',(76.1545922983369,2.13994607088214,330.569601604476));
#60310=CARTESIAN_POINT('Ctrl Pts',(76.1468172195584,2.01597568064073,330.511821208261));
#60311=CARTESIAN_POINT('Ctrl Pts',(76.13904214078,1.88964361352443,330.459247851251));
#60312=CARTESIAN_POINT('Ctrl Pts',(76.131276629731,1.76346700605941,330.406739189104));
#60313=CARTESIAN_POINT('Ctrl Pts',(76.123511118682,1.63493486163489,330.359424965631));
#60314=CARTESIAN_POINT('Ctrl Pts',(76.115745607633,1.50451418742548,330.31751987486));
#60315=CARTESIAN_POINT('Ctrl Pts',(76.1079877961108,1.37422282569433,330.275656333107));
#60316=CARTESIAN_POINT('Ctrl Pts',(76.1002299845886,1.24204703026435,330.239191369842));
#60317=CARTESIAN_POINT('Ctrl Pts',(76.0924721730664,1.10847388728327,330.208291671678));
#60318=CARTESIAN_POINT('Ctrl Pts',(76.0847201995433,0.97500126232804,330.177415226516));
#60319=CARTESIAN_POINT('Ctrl Pts',(76.0769682260204,0.840133762161413,330.15209579811));
#60320=CARTESIAN_POINT('Ctrl Pts',(76.0692162524973,0.704373397894159,330.132450187328));
#60321=CARTESIAN_POINT('Ctrl Pts',(76.0614675619397,0.568670528221865,330.112812896475));
#60322=CARTESIAN_POINT('Ctrl Pts',(76.0537188713821,0.432075932559683,330.09884469998));
#60323=CARTESIAN_POINT('Ctrl Pts',(76.0459701808245,0.295101359665762,330.090611214212));
#60324=CARTESIAN_POINT('Ctrl Pts',(76.0382231024466,0.158155285475765,330.082379441489));
#60325=CARTESIAN_POINT('Ctrl Pts',(76.0304760240688,0.0208297812299513,
330.079880029661));
#60326=CARTESIAN_POINT('Ctrl Pts',(76.022728945691,-0.116359137129804,330.083126642499));
#60327=CARTESIAN_POINT('Ctrl Pts',(76.0149818023852,-0.253549205264831,
330.086373282546));
#60328=CARTESIAN_POINT('Ctrl Pts',(76.0072346590793,-0.390602294465687,
330.095366034065));
#60329=CARTESIAN_POINT('Ctrl Pts',(75.9994875157735,-0.527003642767366,
330.110066439816));
#60330=CARTESIAN_POINT('Ctrl Pts',(75.9917386307454,-0.663435656987934,
330.124770150531));
#60331=CARTESIAN_POINT('Ctrl Pts',(75.9839897457174,-0.799215250192649,
330.145184027033));
#60332=CARTESIAN_POINT('Ctrl Pts',(75.9762408606893,-0.933834421265835,
330.171217924139));
#60333=CARTESIAN_POINT('Ctrl Pts',(75.9684837509146,-1.06859647851817,330.197279453892));
#60334=CARTESIAN_POINT('Ctrl Pts',(75.9607266411398,-1.20219526886451,330.22897284586));
#60335=CARTESIAN_POINT('Ctrl Pts',(75.9529695313651,-1.3341340607493,330.266157018822));
#60336=CARTESIAN_POINT('Ctrl Pts',(75.9452082764389,-1.46614335650588,330.303361061817));
#60337=CARTESIAN_POINT('Ctrl Pts',(75.9374470215127,-1.59649051501126,330.346061610639));
#60338=CARTESIAN_POINT('Ctrl Pts',(75.9296857665866,-1.72469649531938,330.394068491441));
#60339=CARTESIAN_POINT('Ctrl Pts',(75.9219120961819,-1.85310756341376,330.442152167608));
#60340=CARTESIAN_POINT('Ctrl Pts',(75.9141384257772,-1.97937024858825,330.495558985745));
#60341=CARTESIAN_POINT('Ctrl Pts',(75.9063647553725,-2.10302711579265,330.554051280914));
#60342=CARTESIAN_POINT('Ctrl Pts',(75.8989529511955,-2.2209277260784,330.609820745671));
#60343=CARTESIAN_POINT('Ctrl Pts',(75.8915411470184,-2.33645940539615,330.6702127511));
#60344=CARTESIAN_POINT('Ctrl Pts',(75.8841293428413,-2.44925005980186,330.734984500959));
#60345=CARTESIAN_POINT('Ctrl Pts',(75.8763542640629,-2.56756892016618,330.802930907224));
#60346=CARTESIAN_POINT('Ctrl Pts',(75.8685791852845,-2.68324517961335,330.875911965339));
#60347=CARTESIAN_POINT('Ctrl Pts',(75.8608041065061,-2.79582076757547,330.953696835617));
#60348=CARTESIAN_POINT('Ctrl Pts',(75.8530385954571,-2.9082578241096,331.03138598666));
#60349=CARTESIAN_POINT('Ctrl Pts',(75.845273084408,-3.01760148255341,331.113866967809));
#60350=CARTESIAN_POINT('Ctrl Pts',(75.837507573359,-3.12341847774077,331.200863246024));
#60351=CARTESIAN_POINT('Ctrl Pts',(75.8297497618368,-3.22913055506932,331.287773267177));
#60352=CARTESIAN_POINT('Ctrl Pts',(75.8219919503146,-3.33132262777733,331.379189429419));
#60353=CARTESIAN_POINT('Ctrl Pts',(75.8142341387924,-3.4295909352723,331.474792335309));
#60354=CARTESIAN_POINT('Ctrl Pts',(75.8064821652694,-3.52778529274962,331.57032329698));
#60355=CARTESIAN_POINT('Ctrl Pts',(75.7987301917464,-3.62206148329866,331.670034459603));
#60356=CARTESIAN_POINT('Ctrl Pts',(75.7909782182234,-3.71204961955839,331.773566878977));
#60357=CARTESIAN_POINT('Ctrl Pts',(75.7832295276658,-3.80199964578894,331.877055452309));
#60358=CARTESIAN_POINT('Ctrl Pts',(75.7754808371082,-3.88766497372865,331.984361769301));
#60359=CARTESIAN_POINT('Ctrl Pts',(75.7677321465506,-3.96871348855744,332.095090998285));
#60360=CARTESIAN_POINT('Ctrl Pts',(75.7599850681728,-4.04974514056586,332.205797189129));
#60361=CARTESIAN_POINT('Ctrl Pts',(75.752237989795,-4.12616165937756,332.319924560204));
#60362=CARTESIAN_POINT('Ctrl Pts',(75.7444909114171,-4.19767230900181,332.437046576947));
#60363=CARTESIAN_POINT('Ctrl Pts',(75.7367437681113,-4.26918355795408,332.554169575285));
#60364=CARTESIAN_POINT('Ctrl Pts',(75.7289966248056,-4.33578865202132,332.674286935744));
#60365=CARTESIAN_POINT('Ctrl Pts',(75.7212494814998,-4.39724136347907,332.796944972587));
#60366=CARTESIAN_POINT('Ctrl Pts',(75.7135005964717,-4.45870789081106,332.919630585561));
#60367=CARTESIAN_POINT('Ctrl Pts',(75.7057517114436,-4.51501955546467,333.044857662141));
#60368=CARTESIAN_POINT('Ctrl Pts',(75.6980028264155,-4.56597725389353,333.172150230619));
#60369=CARTESIAN_POINT('Ctrl Pts',(75.6902457166408,-4.61698903934999,333.299577908744));
#60370=CARTESIAN_POINT('Ctrl Pts',(75.682488606866,-4.66263536124889,333.429075094712));
#60371=CARTESIAN_POINT('Ctrl Pts',(75.6747314970913,-4.70276604785067,333.560147729216));
#60372=CARTESIAN_POINT('Ctrl Pts',(75.6669702421651,-4.74291817900828,333.691290404744));
#60373=CARTESIAN_POINT('Ctrl Pts',(75.659208987239,-4.77754870331365,333.824009828291));
#60374=CARTESIAN_POINT('Ctrl Pts',(75.6514477323128,-4.80655830546722,333.957800250123));
#60375=CARTESIAN_POINT('Ctrl Pts',(75.6436740619082,-4.83561431353001,334.091804693028));
#60376=CARTESIAN_POINT('Ctrl Pts',(75.6359003915035,-4.85903136467351,334.226883172464));
#60377=CARTESIAN_POINT('Ctrl Pts',(75.6281267210988,-4.87676177206106,334.362522407403));
#60378=CARTESIAN_POINT('Ctrl Pts',(75.6207149169217,-4.89366682471911,334.491847603323));
#60379=CARTESIAN_POINT('Ctrl Pts',(75.6133031127446,-4.90540271983216,334.621682236652));
#60380=CARTESIAN_POINT('Ctrl Pts',(75.6058913085675,-4.91197226855648,334.751582014677));
#60381=CARTESIAN_POINT('Ctrl Pts',(75.6011999978812,-4.91613047260478,334.833802240985));
#60382=CARTESIAN_POINT('Ctrl Pts',(75.5965086871949,-4.91822444166389,334.916127743892));
#60383=CARTESIAN_POINT('Ctrl Pts',(75.5918173765086,-4.91824976747175,334.998487629658));
#60384=CARTESIAN_POINT('',(73.8418173765086,-4.91570827891568,334.996279922712));
#60385=CARTESIAN_POINT('Ctrl Pts',(75.5918173764531,-4.91824976747205,334.998487630632));
#60386=CARTESIAN_POINT('Ctrl Pts',(75.5841035836817,-4.9182914099726,335.133909719248));
#60387=CARTESIAN_POINT('Ctrl Pts',(75.5763897909102,-4.9127356297837,335.269558694198));
#60388=CARTESIAN_POINT('Ctrl Pts',(75.5686759981387,-4.90155235995752,335.40492903711));
#60389=CARTESIAN_POINT('Ctrl Pts',(75.5609714749913,-4.89038252900765,335.540136706195));
#60390=CARTESIAN_POINT('Ctrl Pts',(75.5532669518439,-4.87359869244814,335.675066016892));
#60391=CARTESIAN_POINT('Ctrl Pts',(75.5455624286965,-4.85122276368811,335.80920996013));
#60392=CARTESIAN_POINT('Ctrl Pts',(75.537865249435,-4.82886816347314,335.943226038502));
#60393=CARTESIAN_POINT('Ctrl Pts',(75.5301680701736,-4.80093214085618,336.076457849102));
#60394=CARTESIAN_POINT('Ctrl Pts',(75.5224708909121,-4.76748849417152,336.208402466251));
#60395=CARTESIAN_POINT('Ctrl Pts',(75.5147791369368,-4.73406841993406,336.340254083449));
#60396=CARTESIAN_POINT('Ctrl Pts',(75.5070873829615,-4.69514854401216,336.47081992869));
#60397=CARTESIAN_POINT('Ctrl Pts',(75.4993956289861,-4.65085384591263,336.599606691177));
#60398=CARTESIAN_POINT('Ctrl Pts',(75.4917065716272,-4.60657467688655,336.728348302909));
#60399=CARTESIAN_POINT('Ctrl Pts',(75.4840175142683,-4.5569245600251,336.855311696267));
#60400=CARTESIAN_POINT('Ctrl Pts',(75.4763284569095,-4.50207841063051,336.980018446135));
#60401=CARTESIAN_POINT('Ctrl Pts',(75.4686405336803,-4.44724035099847,337.104706801858));
#60402=CARTESIAN_POINT('Ctrl Pts',(75.4609526104512,-4.38720794289566,337.227138812183));
#60403=CARTESIAN_POINT('Ctrl Pts',(75.453264687222,-4.32220415378727,337.346856262212));
#60404=CARTESIAN_POINT('Ctrl Pts',(75.4455761693606,-4.25719533687747,337.466582971941));
#60405=CARTESIAN_POINT('Ctrl Pts',(75.4378876514992,-4.18721456394206,337.583594354393));
#60406=CARTESIAN_POINT('Ctrl Pts',(75.4301991336378,-4.11253040421546,337.697457457849));
#60407=CARTESIAN_POINT('Ctrl Pts',(75.4225082922612,-4.03782367449748,337.811354971402));
#60408=CARTESIAN_POINT('Ctrl Pts',(75.4148174508845,-3.95841094874331,337.922101981285));
#60409=CARTESIAN_POINT('Ctrl Pts',(75.4071266095078,-3.87460340375593,338.029295549481));
#60410=CARTESIAN_POINT('Ctrl Pts',(75.3994274343602,-3.79070504518257,338.136605272282));
#60411=CARTESIAN_POINT('Ctrl Pts',(75.3917282592126,-3.7024026052751,338.240353553016));
#60412=CARTESIAN_POINT('Ctrl Pts',(75.384029084065,-3.61004696285084,338.340171251375));
#60413=CARTESIAN_POINT('Ctrl Pts',(75.3763251424456,-3.51763414409775,338.440050745736));
#60414=CARTESIAN_POINT('Ctrl Pts',(75.3686212008261,-3.42116340737893,338.535994532661));
#60415=CARTESIAN_POINT('Ctrl Pts',(75.3609172592066,-3.32102069540787,338.627672063896));
#60416=CARTESIAN_POINT('Ctrl Pts',(75.3532021529419,-3.22073285540919,338.719482455317));
#60417=CARTESIAN_POINT('Ctrl Pts',(75.3454870466773,-3.1167627199582,338.807013993407));
#60418=CARTESIAN_POINT('Ctrl Pts',(75.3377719404126,-3.00952764492679,338.889977688486));
#60419=CARTESIAN_POINT('Ctrl Pts',(75.3343990517063,-2.96264663498534,338.926247741103));
#60420=CARTESIAN_POINT('Ctrl Pts',(75.3310261629999,-2.91514196248135,338.96164533264));
#60421=CARTESIAN_POINT('Ctrl Pts',(75.3276532742936,-2.86705002705022,338.996149046881));
#60422=CARTESIAN_POINT('Ctrl Pts',(75.3198781955152,-2.75618998417827,339.075685942324));
#60423=CARTESIAN_POINT('Ctrl Pts',(75.3121031167368,-2.6418425179937,339.150731853742));
#60424=CARTESIAN_POINT('Ctrl Pts',(75.3043280379583,-2.52440750273015,339.220965508348));
#60425=CARTESIAN_POINT('Ctrl Pts',(75.2965625269093,-2.40711699872915,339.29111273597));
#60426=CARTESIAN_POINT('Ctrl Pts',(75.2887970158603,-2.28674683766816,339.356459290732));
#60427=CARTESIAN_POINT('Ctrl Pts',(75.2810315048113,-2.16372820438564,339.41672540691));
#60428=CARTESIAN_POINT('Ctrl Pts',(75.2732736932891,-2.04083154443618,339.476931769058));
#60429=CARTESIAN_POINT('Ctrl Pts',(75.2655158817669,-1.91529198684467,339.53206754622));
#60430=CARTESIAN_POINT('Ctrl Pts',(75.2577580702447,-1.78756750545706,339.581897584619));
#60431=CARTESIAN_POINT('Ctrl Pts',(75.2500060967217,-1.65993914079234,339.631690124333));
#60432=CARTESIAN_POINT('Ctrl Pts',(75.2422541231987,-1.53012948775663,339.676184731138));
#60433=CARTESIAN_POINT('Ctrl Pts',(75.2345021496757,-1.39861847975301,339.715193464811));
#60434=CARTESIAN_POINT('Ctrl Pts',(75.2267534591181,-1.26716316673918,339.754185678262));
#60435=CARTESIAN_POINT('Ctrl Pts',(75.2190047685604,-1.13400830578722,339.787696528479));
#60436=CARTESIAN_POINT('Ctrl Pts',(75.2112560780028,-0.999650843911134,
339.815587321684));
#60437=CARTESIAN_POINT('Ctrl Pts',(75.203508999625,-0.865321336227263,339.843472311977));
#60438=CARTESIAN_POINT('Ctrl Pts',(75.1957619212471,-0.729790107781947,
339.865739491681));
#60439=CARTESIAN_POINT('Ctrl Pts',(75.1880148428693,-0.59356581657329,339.882300962036));
#60440=CARTESIAN_POINT('Ctrl Pts',(75.1802676995635,-0.457340383673773,
339.898862571192));
#60441=CARTESIAN_POINT('Ctrl Pts',(75.1725205562577,-0.320422264442621,
339.909718328448));
#60442=CARTESIAN_POINT('Ctrl Pts',(75.1647734129519,-0.183326388630315,
339.914832092527));
#60443=CARTESIAN_POINT('Ctrl Pts',(75.1570245279238,-0.046199690754497,
339.919947006289));
#60444=CARTESIAN_POINT('Ctrl Pts',(75.1492756428957,0.0911044526989541,
339.919317343516));
#60445=CARTESIAN_POINT('Ctrl Pts',(75.1415267578676,0.228070352015549,339.912959085626));
#60446=CARTESIAN_POINT('Ctrl Pts',(75.1337696480928,0.365181628352708,339.906594079015));
#60447=CARTESIAN_POINT('Ctrl Pts',(75.1260125383181,0.501953552314713,339.894488349291));
#60448=CARTESIAN_POINT('Ctrl Pts',(75.1182554285434,0.637874244230223,339.876709906386));
#60449=CARTESIAN_POINT('Ctrl Pts',(75.1104941736172,0.773867567817685,339.858921963251));
#60450=CARTESIAN_POINT('Ctrl Pts',(75.102732918691,0.909008368070891,339.835455333603));
#60451=CARTESIAN_POINT('Ctrl Pts',(75.0949716637648,1.04279519506601,339.806429157248));
#60452=CARTESIAN_POINT('Ctrl Pts',(75.0871979933601,1.1767960373833,339.777356548471));
#60453=CARTESIAN_POINT('Ctrl Pts',(75.0794243229555,1.30943819991849,339.742706720059));
#60454=CARTESIAN_POINT('Ctrl Pts',(75.0716506525508,1.44023476773872,339.702648921225));
#60455=CARTESIAN_POINT('Ctrl Pts',(75.0642388483737,1.56494272385971,339.664455822563));
#60456=CARTESIAN_POINT('Ctrl Pts',(75.0568270441966,1.68797277171648,339.621347000145));
#60457=CARTESIAN_POINT('Ctrl Pts',(75.0494152400194,1.80892170669439,339.573509081827));
#60458=CARTESIAN_POINT('Ctrl Pts',(75.041640161241,1.9357987092633,339.52332648463));
#60459=CARTESIAN_POINT('Ctrl Pts',(75.0338650824626,2.06078639241786,339.467780909621));
#60460=CARTESIAN_POINT('Ctrl Pts',(75.0260900036841,2.18339819612375,339.407034760433));
#60461=CARTESIAN_POINT('Ctrl Pts',(75.0183244926351,2.30585911819908,339.346363363249));
#60462=CARTESIAN_POINT('Ctrl Pts',(75.0105589815861,2.42594963119493,339.280504297194));
#60463=CARTESIAN_POINT('Ctrl Pts',(75.0027934705371,2.54320113528671,339.209668757512));
#60464=CARTESIAN_POINT('Ctrl Pts',(74.9950356590149,2.66033638417081,339.138903451474));
#60465=CARTESIAN_POINT('Ctrl Pts',(74.9872778474927,2.77463789352716,339.063171691939));
#60466=CARTESIAN_POINT('Ctrl Pts',(74.9795200359705,2.88566008160159,338.982731343683));
#60467=CARTESIAN_POINT('Ctrl Pts',(74.9717680624475,2.99659872195855,338.902351529339));
#60468=CARTESIAN_POINT('Ctrl Pts',(74.9640160889245,3.1042626378053,338.817270407576));
#60469=CARTESIAN_POINT('Ctrl Pts',(74.9562641154015,3.20823406669626,338.727789859392));
#60470=CARTESIAN_POINT('Ctrl Pts',(74.9485154248439,3.31216146362564,338.638347206274));
#60471=CARTESIAN_POINT('Ctrl Pts',(74.9407667342863,3.41239918818163,338.54450908687));
#60472=CARTESIAN_POINT('Ctrl Pts',(74.9330180437287,3.50856168326241,338.446618339364));
#60473=CARTESIAN_POINT('Ctrl Pts',(74.9252709653508,3.60470417093292,338.348747958846));
#60474=CARTESIAN_POINT('Ctrl Pts',(74.9175238869729,3.69677284188704,338.246826906043));
#60475=CARTESIAN_POINT('Ctrl Pts',(74.9097768085951,3.78441851615346,338.141235355254));
#60476=CARTESIAN_POINT('Ctrl Pts',(74.9020296652893,3.872064924975,338.035642919506));
#60477=CARTESIAN_POINT('Ctrl Pts',(74.8942825219835,3.95528801352465,337.926380225179));
#60478=CARTESIAN_POINT('Ctrl Pts',(74.8865353786777,4.03377873179762,337.813860729567));
#60479=CARTESIAN_POINT('Ctrl Pts',(74.8787864936496,4.11228709645053,337.701315937183));
#60480=CARTESIAN_POINT('Ctrl Pts',(74.8710376086215,4.18606075012456,337.585513207041));
#60481=CARTESIAN_POINT('Ctrl Pts',(74.8632887235934,4.25483406263886,337.466894842086));
#60482=CARTESIAN_POINT('Ctrl Pts',(74.8555316138187,4.32368037185762,337.348150574372));
#60483=CARTESIAN_POINT('Ctrl Pts',(74.8477745040439,4.38751554149542,337.22658504063));
#60484=CARTESIAN_POINT('Ctrl Pts',(74.8400173942692,4.44611975509398,337.102665495475));
#60485=CARTESIAN_POINT('Ctrl Pts',(74.832256139343,4.50475528491052,336.978679731678));
#60486=CARTESIAN_POINT('Ctrl Pts',(74.8244948844169,4.55815413679541,336.852337809825));
#60487=CARTESIAN_POINT('Ctrl Pts',(74.8167336294907,4.60614513462613,336.724125883241));
#60488=CARTESIAN_POINT('Ctrl Pts',(74.808959959086,4.65421290241309,336.595708859358));
#60489=CARTESIAN_POINT('Ctrl Pts',(74.8011862886813,4.6968554076331,336.465416224725));
#60490=CARTESIAN_POINT('Ctrl Pts',(74.7934126182767,4.73395147795044,336.333749026958));
#60491=CARTESIAN_POINT('Ctrl Pts',(74.7860008140996,4.76932071726955,336.208210968924));
#60492=CARTESIAN_POINT('Ctrl Pts',(74.7785890099226,4.79964820716896,336.081423719557));
#60493=CARTESIAN_POINT('Ctrl Pts',(74.7711772057455,4.82487268984287,335.953827337262));
#60494=CARTESIAN_POINT('Ctrl Pts',(74.7634021269671,4.85133349955259,335.81997707618));
#60495=CARTESIAN_POINT('Ctrl Pts',(74.7556270481887,4.87226204766127,335.684813369079));
#60496=CARTESIAN_POINT('Ctrl Pts',(74.7478519694102,4.88753159729575,335.548833260595));
#60497=CARTESIAN_POINT('Ctrl Pts',(74.7400864583612,4.90278235677729,335.413020484292));
#60498=CARTESIAN_POINT('Ctrl Pts',(74.7323209473122,4.91238793046495,335.276393690261));
#60499=CARTESIAN_POINT('Ctrl Pts',(74.7245554362632,4.91627233069051,335.139461223955));
#60500=CARTESIAN_POINT('Ctrl Pts',(74.716797624741,4.92015287952192,335.002664526588));
#60501=CARTESIAN_POINT('Ctrl Pts',(74.7090398132189,4.91832353259448,334.865563148282));
#60502=CARTESIAN_POINT('Ctrl Pts',(74.7012820016967,4.91076000404486,334.728671333668));
#60503=CARTESIAN_POINT('Ctrl Pts',(74.6935300281737,4.90320216729032,334.591882534486));
#60504=CARTESIAN_POINT('Ctrl Pts',(74.6857780546507,4.88991875949252,334.455303373801));
#60505=CARTESIAN_POINT('Ctrl Pts',(74.6780260811277,4.87093756359354,334.319448522099));
#60506=CARTESIAN_POINT('Ctrl Pts',(74.67027739057,4.85196440624227,334.183651205006));
#60507=CARTESIAN_POINT('Ctrl Pts',(74.6625287000124,4.82729831408367,334.04857797311));
#60508=CARTESIAN_POINT('Ctrl Pts',(74.6547800094548,4.79701893998964,333.914738579014));
#60509=CARTESIAN_POINT('Ctrl Pts',(74.647032931077,4.76674586577233,333.780927031322));
#60510=CARTESIAN_POINT('Ctrl Pts',(74.6392858526991,4.730861918832,333.648349191817));
#60511=CARTESIAN_POINT('Ctrl Pts',(74.6315387743213,4.68949783452994,333.517504427514));
#60512=CARTESIAN_POINT('Ctrl Pts',(74.6237916310155,4.64813340355697,333.386658566606));
#60513=CARTESIAN_POINT('Ctrl Pts',(74.6160444877097,4.60128886143401,333.257546182566));
#60514=CARTESIAN_POINT('Ctrl Pts',(74.6082973444039,4.54914464852978,333.130650907601));
#60515=CARTESIAN_POINT('Ctrl Pts',(74.6005484593758,4.49698871249951,333.003727103885));
#60516=CARTESIAN_POINT('Ctrl Pts',(74.5927995743478,4.43953088331497,332.879021762579));
#60517=CARTESIAN_POINT('Ctrl Pts',(74.5850506893197,4.37699935522521,332.756997613274));
#60518=CARTESIAN_POINT('Ctrl Pts',(74.5772935795449,4.31440145552538,332.634843946276));
#60519=CARTESIAN_POINT('Ctrl Pts',(74.5695364697702,4.24671927786793,332.515377504528));
#60520=CARTESIAN_POINT('Ctrl Pts',(74.5617793599955,4.17422679132692,332.399035994661));
#60521=CARTESIAN_POINT('Ctrl Pts',(74.5540181050693,4.10169556711892,332.282632315612));
#60522=CARTESIAN_POINT('Ctrl Pts',(74.5462568501431,4.02434913242652,332.169357218434));
#60523=CARTESIAN_POINT('Ctrl Pts',(74.538495595217,3.94250367072959,332.059617734242));
#60524=CARTESIAN_POINT('Ctrl Pts',(74.5307219248123,3.86052728296742,331.949702702639));
#60525=CARTESIAN_POINT('Ctrl Pts',(74.5229482544076,3.77403773323438,331.843334889472));
#60526=CARTESIAN_POINT('Ctrl Pts',(74.515174584003,3.68339078985592,331.740887336758));
#60527=CARTESIAN_POINT('Ctrl Pts',(74.5077627798259,3.59696348349987,331.64320874227));
#60528=CARTESIAN_POINT('Ctrl Pts',(74.5003509756488,3.5067573255949,331.549093853321));
#60529=CARTESIAN_POINT('Ctrl Pts',(74.4929391714717,3.41310922052829,331.45883232376));
#60530=CARTESIAN_POINT('Ctrl Pts',(74.4851640926932,3.31487114286913,331.364146807761));
#60531=CARTESIAN_POINT('Ctrl Pts',(74.4773890139148,3.21253473623743,331.273402707561));
#60532=CARTESIAN_POINT('Ctrl Pts',(74.4696139351363,3.10644939147907,331.186975578274));
#60533=CARTESIAN_POINT('Ctrl Pts',(74.4618484240873,3.00049459149102,331.100654803072));
#60534=CARTESIAN_POINT('Ctrl Pts',(74.4540829130383,2.89080033267491,331.018640673338));
#60535=CARTESIAN_POINT('Ctrl Pts',(74.4463174019892,2.77775297228042,330.941272183616));
#60536=CARTESIAN_POINT('Ctrl Pts',(74.4385595904671,2.66481769867343,330.863980404978));
#60537=CARTESIAN_POINT('Ctrl Pts',(74.4308017789449,2.54853626013645,330.79132531916));
#60538=CARTESIAN_POINT('Ctrl Pts',(74.4230439674227,2.42932795347532,330.72360563594));
#60539=CARTESIAN_POINT('Ctrl Pts',(74.4152919938997,2.31020935484501,330.655936913929));
#60540=CARTESIAN_POINT('Ctrl Pts',(74.4075400203767,2.18816861067551,330.593196394178));
#60541=CARTESIAN_POINT('Ctrl Pts',(74.3997880468537,2.06365355330069,330.53563923115));
#60542=CARTESIAN_POINT('Ctrl Pts',(74.392039356296,1.93919122812675,330.478106443614));
#60543=CARTESIAN_POINT('Ctrl Pts',(74.3842906657384,1.81225702795665,330.425752810458));
#60544=CARTESIAN_POINT('Ctrl Pts',(74.3765419751808,1.68332271937117,330.378787206268));
#60545=CARTESIAN_POINT('Ctrl Pts',(74.368794896803,1.55441523664511,330.331831373664));
#60546=CARTESIAN_POINT('Ctrl Pts',(74.3610478184251,1.42350884027096,330.290261473926));
#60547=CARTESIAN_POINT('Ctrl Pts',(74.3533007400472,1.29109420703118,330.254237805044));
#60548=CARTESIAN_POINT('Ctrl Pts',(74.3455535967414,1.15867846402932,330.21821383425));
#60549=CARTESIAN_POINT('Ctrl Pts',(74.3378064534356,1.02475483611541,330.187736289634));
#60550=CARTESIAN_POINT('Ctrl Pts',(74.3300593101298,0.889827666568586,330.16291515618));
#60551=CARTESIAN_POINT('Ctrl Pts',(74.3223104251017,0.754870162529831,330.138088442409));
#60552=CARTESIAN_POINT('Ctrl Pts',(74.3145615400736,0.618909052253251,330.118920741008));
#60553=CARTESIAN_POINT('Ctrl Pts',(74.3068126550455,0.482456943923607,330.105470568097));
#60554=CARTESIAN_POINT('Ctrl Pts',(74.2990555452708,0.345860003916089,330.092006119034));
#60555=CARTESIAN_POINT('Ctrl Pts',(74.2912984354961,0.208771414412195,330.084271359549));
#60556=CARTESIAN_POINT('Ctrl Pts',(74.2835413257213,0.0717075126428193,
330.082272771378));
#60557=CARTESIAN_POINT('Ctrl Pts',(74.2757800707952,-0.0654296316929282,
330.080273115225));
#60558=CARTESIAN_POINT('Ctrl Pts',(74.268018815869,-0.202541671476678,330.084015727465));
#60559=CARTESIAN_POINT('Ctrl Pts',(74.2602575609429,-0.339115220538798,
330.093454990556));
#60560=CARTESIAN_POINT('Ctrl Pts',(74.2524838905382,-0.475907242770296,
330.102909353391));
#60561=CARTESIAN_POINT('Ctrl Pts',(74.2447102201335,-0.612158664250082,
330.118078533847));
#60562=CARTESIAN_POINT('Ctrl Pts',(74.2369365497289,-0.747363259332668,
330.138865233189));
#60563=CARTESIAN_POINT('Ctrl Pts',(74.2295247455518,-0.87627404798526,330.158684306675));
#60564=CARTESIAN_POINT('Ctrl Pts',(74.2221129413748,-1.00423299402524,330.1836096226));
#60565=CARTESIAN_POINT('Ctrl Pts',(74.2147011371977,-1.13081420305578,330.213514619194));
#60566=CARTESIAN_POINT('Ctrl Pts',(74.2069260584193,-1.26359953420734,330.244885348754));
#60567=CARTESIAN_POINT('Ctrl Pts',(74.1991509796408,-1.39528828569607,330.281835376828));
#60568=CARTESIAN_POINT('Ctrl Pts',(74.1913759008624,-1.5253755697793,330.324274127622));
#60569=CARTESIAN_POINT('Ctrl Pts',(74.1836103898134,-1.65530277317832,330.366660654832));
#60570=CARTESIAN_POINT('Ctrl Pts',(74.1758448787644,-1.78363206226736,330.414522345726));
#60571=CARTESIAN_POINT('Ctrl Pts',(74.1680793677153,-1.90986928922423,330.46771775365));
#60572=CARTESIAN_POINT('Ctrl Pts',(74.1603215561931,-2.03598135160243,330.520860418172));
#60573=CARTESIAN_POINT('Ctrl Pts',(74.1525637446709,-2.16000512191483,330.57932612471));
#60574=CARTESIAN_POINT('Ctrl Pts',(74.1448059331488,-2.28146250317631,330.642923926634));
#60575=CARTESIAN_POINT('Ctrl Pts',(74.1370539596258,-2.40282848390676,330.706473869195));
#60576=CARTESIAN_POINT('Ctrl Pts',(74.1293019861027,-2.52163157484181,330.775148039305));
#60577=CARTESIAN_POINT('Ctrl Pts',(74.1215500125797,-2.6374148633786,330.848707923919));
#60578=CARTESIAN_POINT('Ctrl Pts',(74.1138013220221,-2.75314911762404,330.922236655879));
#60579=CARTESIAN_POINT('Ctrl Pts',(74.1060526314645,-2.86586578385532,331.000646777873));
#60580=CARTESIAN_POINT('Ctrl Pts',(74.0983039409069,-2.97513391501071,331.083654605343));
#60581=CARTESIAN_POINT('Ctrl Pts',(74.0905568625291,-3.08437931201887,331.16664516234));
#60582=CARTESIAN_POINT('Ctrl Pts',(74.0828097841512,-3.19017729004924,331.254231285788));
#60583=CARTESIAN_POINT('Ctrl Pts',(74.0750627057734,-3.29212751773907,331.346087101552));
#60584=CARTESIAN_POINT('Ctrl Pts',(74.0673155624676,-3.39407859986993,331.437943687156));
#60585=CARTESIAN_POINT('Ctrl Pts',(74.0595684191617,-3.49218157694745,331.534069774811));
#60586=CARTESIAN_POINT('Ctrl Pts',(74.0518212758559,-3.58607103116525,331.63410077068));
#60587=CARTESIAN_POINT('Ctrl Pts',(74.0440723908279,-3.67998159372544,331.73415425564));
#60588=CARTESIAN_POINT('Ctrl Pts',(74.0363235057998,-3.76967648097578,331.838114110804));
#60589=CARTESIAN_POINT('Ctrl Pts',(74.0285746207717,-3.85482908376087,331.945580939443));
#60590=CARTESIAN_POINT('Ctrl Pts',(74.020817510997,-3.94007206839863,332.053161834485));
#60591=CARTESIAN_POINT('Ctrl Pts',(74.0130604012223,-4.02076289458544,332.164256831879));
#60592=CARTESIAN_POINT('Ctrl Pts',(74.0053032914475,-4.09661669198922,332.278435240268));
#60593=CARTESIAN_POINT('Ctrl Pts',(73.9975420365214,-4.17251102323696,332.392674661948));
#60594=CARTESIAN_POINT('Ctrl Pts',(73.9897807815952,-4.24356297297313,332.510000443594));
#60595=CARTESIAN_POINT('Ctrl Pts',(73.982019526669,-4.30953307924865,332.629956181552));
#60596=CARTESIAN_POINT('Ctrl Pts',(73.9742458562643,-4.37560871619465,332.750103809598));
#60597=CARTESIAN_POINT('Ctrl Pts',(73.9664721858597,-4.43658609099692,332.872889450669));
#60598=CARTESIAN_POINT('Ctrl Pts',(73.958698515455,-4.49227307649294,332.997834754892));
#60599=CARTESIAN_POINT('Ctrl Pts',(73.9512867112779,-4.5453678194165,333.116963825144));
#60600=CARTESIAN_POINT('Ctrl Pts',(73.9438749071008,-4.59365351748236,333.238055751415));
#60601=CARTESIAN_POINT('Ctrl Pts',(73.9364631029238,-4.63700612328589,333.360683900186));
#60602=CARTESIAN_POINT('Ctrl Pts',(73.9273880990653,-4.69008700016011,333.510829653725));
#60603=CARTESIAN_POINT('Ctrl Pts',(73.9183130952069,-4.73591098356173,333.663667231865));
#60604=CARTESIAN_POINT('Ctrl Pts',(73.9092380913485,-4.77423708957649,333.818541886053));
#60605=CARTESIAN_POINT('Ctrl Pts',(73.9002022728023,-4.81239770580721,333.972747800946));
#60606=CARTESIAN_POINT('Ctrl Pts',(73.891166454256,-4.8431249669467,334.128973136046));
#60607=CARTESIAN_POINT('Ctrl Pts',(73.8821306357098,-4.86622770248834,334.286549924637));
#60608=CARTESIAN_POINT('Ctrl Pts',(73.873167972811,-4.88914339403743,334.44285094259));
#60609=CARTESIAN_POINT('Ctrl Pts',(73.8642053099122,-4.90455744254433,334.600481501425));
#60610=CARTESIAN_POINT('Ctrl Pts',(73.8552426470135,-4.91233052211994,334.758770018553));
#60611=CARTESIAN_POINT('Ctrl Pts',(73.8507675568452,-4.91621164901036,334.837804050599));
#60612=CARTESIAN_POINT('Ctrl Pts',(73.8462924666769,-4.91818859753757,334.917001816555));
#60613=CARTESIAN_POINT('Ctrl Pts',(73.8418173765086,-4.918248591645,334.996278000271));
#60614=CARTESIAN_POINT('',(72.0918173765086,-4.91544128743151,335.003188401032));
#60615=CARTESIAN_POINT('Ctrl Pts',(73.8418173765086,-4.91336535392688,334.996281695775));
#60616=CARTESIAN_POINT('Ctrl Pts',(73.7806199405557,-4.90577526826458,336.079323715111));
#60617=CARTESIAN_POINT('Ctrl Pts',(73.626676493178,-4.01863795453471,338.81503798128));
#60618=CARTESIAN_POINT('Ctrl Pts',(73.3799870343759,0.507402860391596,340.793702719651));
#60619=CARTESIAN_POINT('Ctrl Pts',(73.101749000102,5.14663302270979,337.708619093927));
#60620=CARTESIAN_POINT('Ctrl Pts',(72.823510965828,5.0628740242661,332.137875704857));
#60621=CARTESIAN_POINT('Ctrl Pts',(72.5452729315541,0.332990261651519,329.193661536556));
#60622=CARTESIAN_POINT('Ctrl Pts',(72.3013750684476,-4.0809961841249,331.283583074452));
#60623=CARTESIAN_POINT('Ctrl Pts',(72.1502232167658,-4.90617808429904,333.968985933903));
#60624=CARTESIAN_POINT('Ctrl Pts',(72.0918173765086,-4.91230093438665,335.003186364042));
#60625=CARTESIAN_POINT('',(70.3418173765448,-4.9182494475218,335.002331191005));
#60626=CARTESIAN_POINT('Ctrl Pts',(72.0918173765086,-4.91824896533127,335.003190222232));
#60627=CARTESIAN_POINT('Ctrl Pts',(72.0830646580099,-4.91814831260998,335.158362842285));
#60628=CARTESIAN_POINT('Ctrl Pts',(72.0743119395114,-4.91070000482826,335.3132548513));
#60629=CARTESIAN_POINT('Ctrl Pts',(72.0655592210127,-4.89600773382934,335.467216580167));
#60630=CARTESIAN_POINT('Ctrl Pts',(72.0567713434352,-4.88125644497047,335.621796762898));
#60631=CARTESIAN_POINT('Ctrl Pts',(72.0479834658578,-4.85920298955882,335.775438996226));
#60632=CARTESIAN_POINT('Ctrl Pts',(72.0391955882803,-4.8300021260178,335.927503382831));
#60633=CARTESIAN_POINT('Ctrl Pts',(72.0303584999139,-4.80063774204547,336.080419307065));
#60634=CARTESIAN_POINT('Ctrl Pts',(72.0215214115475,-4.76404577311296,336.231739484791));
#60635=CARTESIAN_POINT('Ctrl Pts',(72.0126843231812,-4.72043232127063,336.380833720186));
#60636=CARTESIAN_POINT('Ctrl Pts',(72.0047218364562,-4.68113526810929,336.515172183364));
#60637=CARTESIAN_POINT('Ctrl Pts',(71.9967593497312,-4.63613847248084,336.647703686998));
#60638=CARTESIAN_POINT('Ctrl Pts',(71.9887968630062,-4.58562526802528,336.777983116834));
#60639=CARTESIAN_POINT('Ctrl Pts',(71.9810217842278,-4.53630096048684,336.905196243233));
#60640=CARTESIAN_POINT('Ctrl Pts',(71.9732467054494,-4.48160103382147,337.030556324065));
#60641=CARTESIAN_POINT('Ctrl Pts',(71.9654716266709,-4.42168460089725,337.153575713247));
#60642=CARTESIAN_POINT('Ctrl Pts',(71.9577061156219,-4.36184189895817,337.276443719239));
#60643=CARTESIAN_POINT('Ctrl Pts',(71.9499406045729,-4.29679563273098,337.396976416642));
#60644=CARTESIAN_POINT('Ctrl Pts',(71.9421750935239,-4.22675382691329,337.514703789549));
#60645=CARTESIAN_POINT('Ctrl Pts',(71.9344172820017,-4.15678146774989,337.632314435424));
#60646=CARTESIAN_POINT('Ctrl Pts',(71.9266594704795,-4.08182362449603,337.747124958366));
#60647=CARTESIAN_POINT('Ctrl Pts',(71.9189016589573,-4.00213514582106,337.85868804473));
#60648=CARTESIAN_POINT('Ctrl Pts',(71.9111496854342,-3.9225066352533,337.970167176334));
#60649=CARTESIAN_POINT('Ctrl Pts',(71.9033977119112,-3.83815480145451,338.078403418836));
#60650=CARTESIAN_POINT('Ctrl Pts',(71.8956457383882,-3.74937869625221,338.182976979903));
#60651=CARTESIAN_POINT('Ctrl Pts',(71.8878970478306,-3.66064018778348,338.287506254004));
#60652=CARTESIAN_POINT('Ctrl Pts',(71.8801483572729,-3.56748138697016,338.388375634434));
#60653=CARTESIAN_POINT('Ctrl Pts',(71.8723996667153,-3.47024251945983,338.485197256775));
#60654=CARTESIAN_POINT('Ctrl Pts',(71.8646525883375,-3.3730238833081,338.581998734569));
#60655=CARTESIAN_POINT('Ctrl Pts',(71.8569055099596,-3.27172714577507,338.674753853786));
#60656=CARTESIAN_POINT('Ctrl Pts',(71.8491584315818,-3.16673011352601,338.763110874076));
#60657=CARTESIAN_POINT('Ctrl Pts',(71.841411288276,-3.06173220130083,338.851468634883));
#60658=CARTESIAN_POINT('Ctrl Pts',(71.8336641449702,-2.95303423157426,338.935427971568));
#60659=CARTESIAN_POINT('Ctrl Pts',(71.8259170016644,-2.84104756435277,339.014677047981));
#60660=CARTESIAN_POINT('Ctrl Pts',(71.8181681166363,-2.72903572015086,339.093943941269));
#60661=CARTESIAN_POINT('Ctrl Pts',(71.8104192316083,-2.61373402619343,339.168498241314));
#60662=CARTESIAN_POINT('Ctrl Pts',(71.8026703465802,-2.49558298081014,339.238071335925));
#60663=CARTESIAN_POINT('Ctrl Pts',(71.7949132368054,-2.37730652868638,339.307718276138));
#60664=CARTESIAN_POINT('Ctrl Pts',(71.7871561270307,-2.25617502110136,339.372373250785));
#60665=CARTESIAN_POINT('Ctrl Pts',(71.779399017256,-2.13265421698883,339.431813291787));
#60666=CARTESIAN_POINT('Ctrl Pts',(71.7716377623298,-2.0090674073081,339.491285095646));
#60667=CARTESIAN_POINT('Ctrl Pts',(71.7638765074036,-1.883089115852,339.5455362586));
#60668=CARTESIAN_POINT('Ctrl Pts',(71.7561152524775,-1.75520432843398,339.594392324121));
#60669=CARTESIAN_POINT('Ctrl Pts',(71.7483415820728,-1.62711496703365,339.643326543425));
#60670=CARTESIAN_POINT('Ctrl Pts',(71.7405679116682,-1.49711338617319,339.686848295053));
#60671=CARTESIAN_POINT('Ctrl Pts',(71.7327942412635,-1.36569980342865,339.724833024501));
#60672=CARTESIAN_POINT('Ctrl Pts',(71.7253824370864,-1.24040355457688,339.761049555655));
#60673=CARTESIAN_POINT('Ctrl Pts',(71.7179706329093,-1.11382408229163,339.792232891618));
#60674=CARTESIAN_POINT('Ctrl Pts',(71.7105588287322,-0.986401021095636,
339.818318803077));
#60675=CARTESIAN_POINT('Ctrl Pts',(71.7027837499537,-0.852732576096907,
339.845683262761));
#60676=CARTESIAN_POINT('Ctrl Pts',(71.6950086711753,-0.717713340685445,
339.867524460355));
#60677=CARTESIAN_POINT('Ctrl Pts',(71.6872335923969,-0.581839491958865,
339.883712303985));
#60678=CARTESIAN_POINT('Ctrl Pts',(71.6794680813478,-0.446132844653388,
339.899880227444));
#60679=CARTESIAN_POINT('Ctrl Pts',(71.6717025702988,-0.309574060945946,
339.910408593201));
#60680=CARTESIAN_POINT('Ctrl Pts',(71.6639370592498,-0.172670961339019,
339.915217981088));
#60681=CARTESIAN_POINT('Ctrl Pts',(71.6561792477276,-0.0359036015540283,
339.920022600453));
#60682=CARTESIAN_POINT('Ctrl Pts',(71.6484214362055,0.101207006627649,339.919119512695));
#60683=CARTESIAN_POINT('Ctrl Pts',(71.6406636246833,0.238146794379776,339.912480958419));
#60684=CARTESIAN_POINT('Ctrl Pts',(71.6329116511603,0.374983530599102,339.905847399865));
#60685=CARTESIAN_POINT('Ctrl Pts',(71.6251596776372,0.511649313413178,339.893486984668));
#60686=CARTESIAN_POINT('Ctrl Pts',(71.6174077041142,0.647629296389616,339.875424018171));
#60687=CARTESIAN_POINT('Ctrl Pts',(71.6096590135566,0.783551691762532,339.857368701351));
#60688=CARTESIAN_POINT('Ctrl Pts',(71.601910322999,0.918788478291488,339.833615687926));
#60689=CARTESIAN_POINT('Ctrl Pts',(71.5941616324414,1.05282937689145,339.804241185209));
#60690=CARTESIAN_POINT('Ctrl Pts',(71.5864145540635,1.18684238716293,339.774872794102));
#60691=CARTESIAN_POINT('Ctrl Pts',(71.5786674756857,1.31965962284119,339.739885323735));
#60692=CARTESIAN_POINT('Ctrl Pts',(71.5709203973079,1.45078084509586,339.699406132907));
#60693=CARTESIAN_POINT('Ctrl Pts',(71.5631732540021,1.58190316627257,339.658926602824));
#60694=CARTESIAN_POINT('Ctrl Pts',(71.5554261106962,1.71132907219253,339.612955375778));
#60695=CARTESIAN_POINT('Ctrl Pts',(71.5476789673904,1.8385737226806,339.561669620738));
#60696=CARTESIAN_POINT('Ctrl Pts',(71.5399300823623,1.96584698046749,339.510372335573));
#60697=CARTESIAN_POINT('Ctrl Pts',(71.5321811973343,2.09093764453166,339.453758290949));
#60698=CARTESIAN_POINT('Ctrl Pts',(71.5244323123062,2.21338145422958,339.392052549842));
#60699=CARTESIAN_POINT('Ctrl Pts',(71.5166752025314,2.33595522705236,339.330281313623));
#60700=CARTESIAN_POINT('Ctrl Pts',(71.5089180927567,2.45587618386523,339.263407761351));
#60701=CARTESIAN_POINT('Ctrl Pts',(71.501160982982,2.57270477716889,339.191702898827));
#60702=CARTESIAN_POINT('Ctrl Pts',(71.4933997280558,2.68959579993728,339.119959719517));
#60703=CARTESIAN_POINT('Ctrl Pts',(71.4856384731296,2.80339084240301,339.043380303808));
#60704=CARTESIAN_POINT('Ctrl Pts',(71.4778772182035,2.91368074669759,338.96227807818));
#60705=CARTESIAN_POINT('Ctrl Pts',(71.4701035477988,3.02414707889566,338.881046115422));
#60706=CARTESIAN_POINT('Ctrl Pts',(71.4623298773941,3.13109676322804,338.795277129697));
#60707=CARTESIAN_POINT('Ctrl Pts',(71.4545562069895,3.23415436272227,338.705324361049));
#60708=CARTESIAN_POINT('Ctrl Pts',(71.4471444028124,3.33241460616541,338.619558915423));
#60709=CARTESIAN_POINT('Ctrl Pts',(71.4397325986354,3.42713675422618,338.529990629114));
#60710=CARTESIAN_POINT('Ctrl Pts',(71.4323207944583,3.51802888363629,338.436954442003));
#60711=CARTESIAN_POINT('Ctrl Pts',(71.4245457156799,3.61337590706287,338.33935827422));
#60712=CARTESIAN_POINT('Ctrl Pts',(71.4167706369015,3.70480929176386,338.237637243919));
#60713=CARTESIAN_POINT('Ctrl Pts',(71.408995558123,3.79195113081103,338.13213819683));
#60714=CARTESIAN_POINT('Ctrl Pts',(71.401230047074,3.87898573627754,338.026768973035));
#60715=CARTESIAN_POINT('Ctrl Pts',(71.393464536025,3.96173905726131,337.91763128129));
#60716=CARTESIAN_POINT('Ctrl Pts',(71.385699024976,4.03986949683469,337.80510917988));
#60717=CARTESIAN_POINT('Ctrl Pts',(71.3779412134538,4.11792246984977,337.69269864446));
#60718=CARTESIAN_POINT('Ctrl Pts',(71.3701834019316,4.19136146158048,337.576910696309));
#60719=CARTESIAN_POINT('Ctrl Pts',(71.3624255904094,4.2598849364179,337.458162604666));
#60720=CARTESIAN_POINT('Ctrl Pts',(71.3546736168864,4.3283568451675,337.339503874729));
#60721=CARTESIAN_POINT('Ctrl Pts',(71.3469216433634,4.39192040529233,337.21788977242));
#60722=CARTESIAN_POINT('Ctrl Pts',(71.3391696698403,4.45031744272701,337.093766396105));
#60723=CARTESIAN_POINT('Ctrl Pts',(71.3314209792827,4.50868974898163,336.969695586114));
#60724=CARTESIAN_POINT('Ctrl Pts',(71.3236722887251,4.56189971832029,336.84311796866));
#60725=CARTESIAN_POINT('Ctrl Pts',(71.3159235981675,4.60973529380511,336.714503888461));
#60726=CARTESIAN_POINT('Ctrl Pts',(71.3081765197897,4.65756091669892,336.585916567496));
#60727=CARTESIAN_POINT('Ctrl Pts',(71.3004294414118,4.70001423371958,336.455293992686));
#60728=CARTESIAN_POINT('Ctrl Pts',(71.292682363034,4.73693163566275,336.323125746691));
#60729=CARTESIAN_POINT('Ctrl Pts',(71.2849352197282,4.7738493470093,336.190956392999));
#60730=CARTESIAN_POINT('Ctrl Pts',(71.2771880764224,4.80523094558301,336.057241718747));
#60731=CARTESIAN_POINT('Ctrl Pts',(71.2694409331166,4.83096304171257,335.922485312678));
#60732=CARTESIAN_POINT('Ctrl Pts',(71.2616920480885,4.85670092296364,335.787698610509));
#60733=CARTESIAN_POINT('Ctrl Pts',(71.2539431630604,4.87678670105804,335.651870094346));
#60734=CARTESIAN_POINT('Ctrl Pts',(71.2461942780323,4.89115839817848,335.515511965359));
#60735=CARTESIAN_POINT('Ctrl Pts',(71.2384371682576,4.90554534956675,335.379009104445));
#60736=CARTESIAN_POINT('Ctrl Pts',(71.2306800584828,4.91420606357072,335.241975897121));
#60737=CARTESIAN_POINT('Ctrl Pts',(71.2229229487081,4.91713057037797,335.104928625048));
#60738=CARTESIAN_POINT('Ctrl Pts',(71.215161693782,4.92005663994815,334.967808119294));
#60739=CARTESIAN_POINT('Ctrl Pts',(71.2074004388558,4.91724040256479,334.830673924407));
#60740=CARTESIAN_POINT('Ctrl Pts',(71.1996391839296,4.90872400644114,334.694039723022));
#60741=CARTESIAN_POINT('Ctrl Pts',(71.1918655135249,4.90019398685918,334.557186951443));
#60742=CARTESIAN_POINT('Ctrl Pts',(71.1840918431203,4.88594562792644,334.420836160618));
#60743=CARTESIAN_POINT('Ctrl Pts',(71.1763181727156,4.86607280624221,334.285494221962));
#60744=CARTESIAN_POINT('Ctrl Pts',(71.1689063685385,4.84712506918852,334.156452483111));
#60745=CARTESIAN_POINT('Ctrl Pts',(71.1614945643615,4.82306477584683,334.028328068849));
#60746=CARTESIAN_POINT('Ctrl Pts',(71.1540827601844,4.79401560787775,333.901547718868));
#60747=CARTESIAN_POINT('Ctrl Pts',(71.146307681406,4.76354265365348,333.768553486275));
#60748=CARTESIAN_POINT('Ctrl Pts',(71.1385326026275,4.72748312005856,333.636618116187));
#60749=CARTESIAN_POINT('Ctrl Pts',(71.1307575238491,4.68592416994429,333.506247096729));
#60750=CARTESIAN_POINT('Ctrl Pts',(71.1229920128001,4.6444163607639,333.37603650711));
#60751=CARTESIAN_POINT('Ctrl Pts',(71.1152265017511,4.59742271779424,333.247386806707));
#60752=CARTESIAN_POINT('Ctrl Pts',(71.1074609907021,4.54508134614102,333.12079308764));
#60753=CARTESIAN_POINT('Ctrl Pts',(71.0997031791799,4.49279187111018,332.994324886614));
#60754=CARTESIAN_POINT('Ctrl Pts',(71.0919453676577,4.43516536763633,332.86990896906));
#60755=CARTESIAN_POINT('Ctrl Pts',(71.0841875561355,4.37238954810552,332.748024711033));
#60756=CARTESIAN_POINT('Ctrl Pts',(71.0764355826125,4.30966096936963,332.626232174776));
#60757=CARTESIAN_POINT('Ctrl Pts',(71.0686836090895,4.24179096587531,332.506967852023));
#60758=CARTESIAN_POINT('Ctrl Pts',(71.0609316355665,4.16901495845334,332.390690256276));
#60759=CARTESIAN_POINT('Ctrl Pts',(71.0531829450089,4.09626977171376,332.27446190416));
#60760=CARTESIAN_POINT('Ctrl Pts',(71.0454342544513,4.01862292037803,332.161218093932));
#60761=CARTESIAN_POINT('Ctrl Pts',(71.0376855638936,3.93635517117736,332.05139167931));
#60762=CARTESIAN_POINT('Ctrl Pts',(71.0299384855158,3.85410453846898,331.94158811499));
#60763=CARTESIAN_POINT('Ctrl Pts',(71.022191407138,3.7672351544122,331.835200844654));
#60764=CARTESIAN_POINT('Ctrl Pts',(71.0144443287601,3.67607018118065,331.732632392042));
#60765=CARTESIAN_POINT('Ctrl Pts',(71.0066971854543,3.58490444389888,331.630063079807));
#60766=CARTESIAN_POINT('Ctrl Pts',(70.9989500421485,3.48944330530694,331.531312941285));
#60767=CARTESIAN_POINT('Ctrl Pts',(70.9912028988427,3.39004888226507,331.436749849035));
#60768=CARTESIAN_POINT('Ctrl Pts',(70.9834540138146,3.29063211324677,331.342165496994));
#60769=CARTESIAN_POINT('Ctrl Pts',(70.9757051287865,3.18728058327983,331.251770333749));
#60770=CARTESIAN_POINT('Ctrl Pts',(70.9679562437584,3.08039147350133,331.165893659211));
#60771=CARTESIAN_POINT('Ctrl Pts',(70.9601991339837,2.97338891051727,331.079925834283));
#60772=CARTESIAN_POINT('Ctrl Pts',(70.952442024209,2.86284157230298,330.998486323662));
#60773=CARTESIAN_POINT('Ctrl Pts',(70.9446849144343,2.7491782158826,330.921862900807));
#60774=CARTESIAN_POINT('Ctrl Pts',(70.9369236595081,2.63545412139888,330.845198532844));
#60775=CARTESIAN_POINT('Ctrl Pts',(70.9291624045819,2.5186110236457,330.77335558533));
#60776=CARTESIAN_POINT('Ctrl Pts',(70.9214011496558,2.39910369812485,330.706576598081));
#60777=CARTESIAN_POINT('Ctrl Pts',(70.9136274792511,2.27940519983042,330.639690786216));
#60778=CARTESIAN_POINT('Ctrl Pts',(70.9058538088465,2.15703430631976,330.577885298496));
#60779=CARTESIAN_POINT('Ctrl Pts',(70.8980801384418,2.03246805859439,330.521355489292));
#60780=CARTESIAN_POINT('Ctrl Pts',(70.8906683342647,1.91370039966878,330.467457156307));
#60781=CARTESIAN_POINT('Ctrl Pts',(70.8832565300876,1.7929374409938,330.418354497947));
#60782=CARTESIAN_POINT('Ctrl Pts',(70.8758447259104,1.67060496832461,330.374174440999));
#60783=CARTESIAN_POINT('Ctrl Pts',(70.868069647132,1.54227661676101,330.327828987854));
#60784=CARTESIAN_POINT('Ctrl Pts',(70.8602945683536,1.41181546661236,330.286754419746));
#60785=CARTESIAN_POINT('Ctrl Pts',(70.8525194895751,1.27969376244737,330.251150988202));
#60786=CARTESIAN_POINT('Ctrl Pts',(70.8447539785261,1.14773464245056,330.215591368947));
#60787=CARTESIAN_POINT('Ctrl Pts',(70.8369884674771,1.01411940805555,330.18548959108));
#60788=CARTESIAN_POINT('Ctrl Pts',(70.8292229564281,0.879339129384364,330.160997441824));
#60789=CARTESIAN_POINT('Ctrl Pts',(70.8214651449059,0.744692485751883,330.136529576605));
#60790=CARTESIAN_POINT('Ctrl Pts',(70.8137073333836,0.608883478745489,330.117660340812));
#60791=CARTESIAN_POINT('Ctrl Pts',(70.8059495218615,0.472416807860145,330.104491300983));
#60792=CARTESIAN_POINT('Ctrl Pts',(70.7981975483385,0.336052832472621,330.091332171274));
#60793=CARTESIAN_POINT('Ctrl Pts',(70.7904455748155,0.199032565806501,330.083864736729));
#60794=CARTESIAN_POINT('Ctrl Pts',(70.7826936012925,0.0618689813671218,
330.082139154913));
#60795=CARTESIAN_POINT('Ctrl Pts',(70.7749449107349,-0.0752365142130927,
330.080414303881));
#60796=CARTESIAN_POINT('Ctrl Pts',(70.7671962201772,-0.212484816818216,
330.084426474049));
#60797=CARTESIAN_POINT('Ctrl Pts',(70.7594475296196,-0.349359991533065,
330.094173804667));
#60798=CARTESIAN_POINT('Ctrl Pts',(70.7517004512418,-0.486206688224612,
330.103919107271));
#60799=CARTESIAN_POINT('Ctrl Pts',(70.743953372864,-0.622680021800037,330.119397169123));
#60800=CARTESIAN_POINT('Ctrl Pts',(70.7362062944861,-0.758266619864602,
330.140554064947));
#60801=CARTESIAN_POINT('Ctrl Pts',(70.7284591511803,-0.893854354275453,
330.161711138087));
#60802=CARTESIAN_POINT('Ctrl Pts',(70.7207120078745,-1.02855495215148,330.188547079867));
#60803=CARTESIAN_POINT('Ctrl Pts',(70.7129648645687,-1.16186309939871,330.220956455445));
#60804=CARTESIAN_POINT('Ctrl Pts',(70.7052159795406,-1.29520121714737,330.253373117338));
#60805=CARTESIAN_POINT('Ctrl Pts',(70.6974670945125,-1.42714588159107,330.29136561409));
#60806=CARTESIAN_POINT('Ctrl Pts',(70.6897182094844,-1.55720523990546,330.334778150687));
#60807=CARTESIAN_POINT('Ctrl Pts',(70.6819610997097,-1.68740264456679,330.378236765798));
#60808=CARTESIAN_POINT('Ctrl Pts',(70.6742039899349,-1.8157103743963,330.427126788732));
#60809=CARTESIAN_POINT('Ctrl Pts',(70.6664468801602,-1.9416544095259,330.481243399289));
#60810=CARTESIAN_POINT('Ctrl Pts',(70.658685625234,-2.06766574512087,330.535388928032));
#60811=CARTESIAN_POINT('Ctrl Pts',(70.6509243703079,-2.19131051703725,330.594766440424));
#60812=CARTESIAN_POINT('Ctrl Pts',(70.6431631153817,-2.31213866325025,330.659124758254));
#60813=CARTESIAN_POINT('Ctrl Pts',(70.6353894449771,-2.43316009511939,330.723586028418));
#60814=CARTESIAN_POINT('Ctrl Pts',(70.6276157745724,-2.55135556042475,330.793043827636));
#60815=CARTESIAN_POINT('Ctrl Pts',(70.6198421041677,-2.6663026272486,330.867202719413));
#60816=CARTESIAN_POINT('Ctrl Pts',(70.6124302999907,-2.77589888045674,330.937909496936));
#60817=CARTESIAN_POINT('Ctrl Pts',(70.6050184958136,-2.88254211974617,331.012889379301));
#60818=CARTESIAN_POINT('Ctrl Pts',(70.5976066916365,-2.98589519257014,331.091853001551));
#60819=CARTESIAN_POINT('Ctrl Pts',(70.5899166867489,-3.09312760402905,331.173780508881));
#60820=CARTESIAN_POINT('Ctrl Pts',(70.5822266818613,-3.19717314114697,331.260268186912));
#60821=CARTESIAN_POINT('Ctrl Pts',(70.5745366769736,-3.2976128294936,331.351036765154));
#60822=CARTESIAN_POINT('Ctrl Pts',(70.5668561735593,-3.39792841843745,331.441693193243));
#60823=CARTESIAN_POINT('Ctrl Pts',(70.5591756701449,-3.49464672559058,331.536619736192));
#60824=CARTESIAN_POINT('Ctrl Pts',(70.5514951667306,-3.58737891189596,331.635494745883));
#60825=CARTESIAN_POINT('Ctrl Pts',(70.543822217071,-3.68001989634226,331.734272512264));
#60826=CARTESIAN_POINT('Ctrl Pts',(70.5361492674113,-3.76868228651825,331.836990730473));
#60827=CARTESIAN_POINT('Ctrl Pts',(70.5284763177517,-3.8530117975947,331.943288834369));
#60828=CARTESIAN_POINT('Ctrl Pts',(70.5206988618681,-3.93848988375168,332.051034727439));
#60829=CARTESIAN_POINT('Ctrl Pts',(70.5129214059844,-4.01951587272606,332.162458473482));
#60830=CARTESIAN_POINT('Ctrl Pts',(70.5051439501008,-4.09576054886704,332.277146976268));
#60831=CARTESIAN_POINT('Ctrl Pts',(70.4974796881985,-4.17089555128226,332.390166289485));
#60832=CARTESIAN_POINT('Ctrl Pts',(70.4898154262962,-4.24138725690919,332.506355619135));
#60833=CARTESIAN_POINT('Ctrl Pts',(70.4821511643939,-4.30696263371713,332.625288241857));
#60834=CARTESIAN_POINT('Ctrl Pts',(70.474488162776,-4.37252722754007,332.744201307715));
#60835=CARTESIAN_POINT('Ctrl Pts',(70.466825161158,-4.43317690716215,332.865856419115));
#60836=CARTESIAN_POINT('Ctrl Pts',(70.4591621595401,-4.48868383873161,332.989800890854));
#60837=CARTESIAN_POINT('Ctrl Pts',(70.4514986713872,-4.54419429451574,333.113753232006));
#60838=CARTESIAN_POINT('Ctrl Pts',(70.4438351832342,-4.59456118986911,333.239994857008));
#60839=CARTESIAN_POINT('Ctrl Pts',(70.4361716950813,-4.63960443655404,333.368052165415));
#60840=CARTESIAN_POINT('Ctrl Pts',(70.4283088352033,-4.68581951904256,333.49944098631));
#60841=CARTESIAN_POINT('Ctrl Pts',(70.4204459753253,-4.72642999964435,333.632740842062));
#60842=CARTESIAN_POINT('Ctrl Pts',(70.4125831154472,-4.76129589053794,333.767423631069));
#60843=CARTESIAN_POINT('Ctrl Pts',(70.4049096326925,-4.79532203581451,333.898862582651));
#60844=CARTESIAN_POINT('Ctrl Pts',(70.3972361499377,-4.82387712552781,334.031618203507));
#60845=CARTESIAN_POINT('Ctrl Pts',(70.389562667183,-4.84688309399061,334.165190239822));
#60846=CARTESIAN_POINT('Ctrl Pts',(70.3816051187433,-4.87074072347867,334.303706997226));
#60847=CARTESIAN_POINT('Ctrl Pts',(70.3736475703036,-4.88863041568758,334.443101301983));
#60848=CARTESIAN_POINT('Ctrl Pts',(70.3656900218639,-4.90052414871174,334.582811636796));
#60849=CARTESIAN_POINT('Ctrl Pts',(70.3577324734242,-4.91241788173591,334.722521971608));
#60850=CARTESIAN_POINT('Ctrl Pts',(70.3497749249845,-4.91831570313657,334.862547861314));
#60851=CARTESIAN_POINT('Ctrl Pts',(70.3418173765448,-4.9182494475218,335.002331191005));
#60852=CARTESIAN_POINT('',(68.5918173764684,-4.91824799793877,334.995562289857));
#60853=CARTESIAN_POINT('Ctrl Pts',(70.3418173765086,-4.9182494475215,335.00233119164));
#60854=CARTESIAN_POINT('Ctrl Pts',(70.3343344701266,-4.91818714382313,335.13377689728));
#60855=CARTESIAN_POINT('Ctrl Pts',(70.3268515637447,-4.91285578162596,335.265093143607));
#60856=CARTESIAN_POINT('Ctrl Pts',(70.3193686573627,-4.90228340698534,335.395980378423));
#60857=CARTESIAN_POINT('Ctrl Pts',(70.3115935785843,-4.89129823070352,335.531978145847));
#60858=CARTESIAN_POINT('Ctrl Pts',(70.3038184998059,-4.87463218996368,335.667733348066));
#60859=CARTESIAN_POINT('Ctrl Pts',(70.2960434210274,-4.85229867721284,335.802733211982));
#60860=CARTESIAN_POINT('Ctrl Pts',(70.2882779099784,-4.82999264727127,335.937566949971));
#60861=CARTESIAN_POINT('Ctrl Pts',(70.2805123989294,-4.80203308513411,336.071646817133));
#60862=CARTESIAN_POINT('Ctrl Pts',(70.2727468878804,-4.76848529200378,336.204462985087));
#60863=CARTESIAN_POINT('Ctrl Pts',(70.2649890763582,-4.73497076160801,336.337147465423));
#60864=CARTESIAN_POINT('Ctrl Pts',(70.2572312648361,-4.69587912172664,336.468570363484));
#60865=CARTESIAN_POINT('Ctrl Pts',(70.2494734533139,-4.65132702810783,336.598230252527));
#60866=CARTESIAN_POINT('Ctrl Pts',(70.2417214797909,-4.60680846135241,336.727792568392));
#60867=CARTESIAN_POINT('Ctrl Pts',(70.2339695062679,-4.55683774645756,336.855594147837));
#60868=CARTESIAN_POINT('Ctrl Pts',(70.2262175327449,-4.50158175651661,336.981147332203));
#60869=CARTESIAN_POINT('Ctrl Pts',(70.2184688421873,-4.44634916752002,337.106647344722));
#60870=CARTESIAN_POINT('Ctrl Pts',(70.2107201516297,-4.38583591245488,337.229900498997));
#60871=CARTESIAN_POINT('Ctrl Pts',(70.202971461072,-4.3202574353507,337.350437992119));
#60872=CARTESIAN_POINT('Ctrl Pts',(70.1952243826942,-4.25469260239645,337.470950406409));
#60873=CARTESIAN_POINT('Ctrl Pts',(70.1874773043164,-4.18406483029078,337.588747940268));
#60874=CARTESIAN_POINT('Ctrl Pts',(70.1797302259385,-4.10863588750571,337.703385693237));
#60875=CARTESIAN_POINT('Ctrl Pts',(70.1719830826327,-4.0332063125535,337.818024406982));
#60876=CARTESIAN_POINT('Ctrl Pts',(70.1642359393269,-3.9529757015129,337.929502960486));
#60877=CARTESIAN_POINT('Ctrl Pts',(70.1564887960212,-3.86824936532322,338.037405127766));
#60878=CARTESIAN_POINT('Ctrl Pts',(70.1487399109931,-3.78350398085437,338.145331553743));
#60879=CARTESIAN_POINT('Ctrl Pts',(70.1409910259649,-3.69426110133613,338.249679686165));
#60880=CARTESIAN_POINT('Ctrl Pts',(70.1332421409368,-3.60086629562431,338.350066414795));
#60881=CARTESIAN_POINT('Ctrl Pts',(70.1254850311621,-3.5073723597007,338.450559694936));
#60882=CARTESIAN_POINT('Ctrl Pts',(70.1177279213874,-3.40971796105718,338.547082885424));
#60883=CARTESIAN_POINT('Ctrl Pts',(70.1099708116127,-3.30828590026031,338.639289417543));
#60884=CARTESIAN_POINT('Ctrl Pts',(70.1022095566865,-3.20679963741346,338.731545221884));
#60885=CARTESIAN_POINT('Ctrl Pts',(70.0944483017604,-3.10153198987717,338.819479521121));
#60886=CARTESIAN_POINT('Ctrl Pts',(70.0866870468342,-2.99289802490024,338.902786757568));
#60887=CARTESIAN_POINT('Ctrl Pts',(70.0789133764296,-2.884090280983,338.986227258444));
#60888=CARTESIAN_POINT('Ctrl Pts',(70.0711397060249,-2.77190577880261,339.065025680773));
#60889=CARTESIAN_POINT('Ctrl Pts',(70.0633660356202,-2.656788419832,339.13891995027));
#60890=CARTESIAN_POINT('Ctrl Pts',(70.055954231443,-2.54702980161509,339.209374423746));
#60891=CARTESIAN_POINT('Ctrl Pts',(70.0485424272658,-2.4346054789703,339.275370900351));
#60892=CARTESIAN_POINT('Ctrl Pts',(70.0411306230886,-2.319918496392,339.33672240668));
#60893=CARTESIAN_POINT('Ctrl Pts',(70.0333555443101,-2.1996103631647,339.401080933089));
#60894=CARTESIAN_POINT('Ctrl Pts',(70.0255804655317,-2.07643196646708,339.460531033429));
#60895=CARTESIAN_POINT('Ctrl Pts',(70.0178053867533,-1.95082175555792,339.514806478748));
#60896=CARTESIAN_POINT('Ctrl Pts',(70.0100398757042,-1.82536611601003,339.569015134676));
#60897=CARTESIAN_POINT('Ctrl Pts',(70.0022743646552,-1.69748497185276,339.618061652006));
#60898=CARTESIAN_POINT('Ctrl Pts',(69.9945088536062,-1.56764238687685,339.661725046522));
#60899=CARTESIAN_POINT('Ctrl Pts',(69.986751042084,-1.43792854120187,339.705345148655));
#60900=CARTESIAN_POINT('Ctrl Pts',(69.9789932305618,-1.3062574930196,339.74359262588));
#60901=CARTESIAN_POINT('Ctrl Pts',(69.9712354190396,-1.17311403189479,339.776294225723));
#60902=CARTESIAN_POINT('Ctrl Pts',(69.9634834455166,-1.04007076544689,339.808971216574));
#60903=CARTESIAN_POINT('Ctrl Pts',(69.9557314719936,-0.905557669614834,
339.836110544232));
#60904=CARTESIAN_POINT('Ctrl Pts',(69.9479794984706,-0.770075131576116,
339.857588635756));
#60905=CARTESIAN_POINT('Ctrl Pts',(69.9402308079129,-0.634649970472694,
339.879057631296));
#60906=CARTESIAN_POINT('Ctrl Pts',(69.9324821173553,-0.49825656898606,339.894870098161));
#60907=CARTESIAN_POINT('Ctrl Pts',(69.9247334267977,-0.36140574261198,339.904953511676));
#60908=CARTESIAN_POINT('Ctrl Pts',(69.9169863484199,-0.224583389195327,
339.915034827254));
#60909=CARTESIAN_POINT('Ctrl Pts',(69.909239270042,-0.0873041897660356,
339.919389431704));
#60910=CARTESIAN_POINT('Ctrl Pts',(69.9014921916642,0.0499160714483651,
339.917996690555));
#60911=CARTESIAN_POINT('Ctrl Pts',(69.8937450483584,0.187137482700722,339.916603937733));
#60912=CARTESIAN_POINT('Ctrl Pts',(69.8859979050526,0.324299563898789,339.909463747203));
#60913=CARTESIAN_POINT('Ctrl Pts',(69.8782507617468,0.460887080464483,339.896607617684));
#60914=CARTESIAN_POINT('Ctrl Pts',(69.8705018767187,0.59750530480355,339.883748597834));
#60915=CARTESIAN_POINT('Ctrl Pts',(69.8627529916906,0.733548318389533,339.865171118482));
#60916=CARTESIAN_POINT('Ctrl Pts',(69.8550041066625,0.868506948514763,339.840958452918));
#60917=CARTESIAN_POINT('Ctrl Pts',(69.8472469968877,1.00360882512458,339.816720087782));
#60918=CARTESIAN_POINT('Ctrl Pts',(69.839489887113,1.1376236337522,339.78683465747));
#60919=CARTESIAN_POINT('Ctrl Pts',(69.8317327773383,1.27005278201869,339.751436518926));
#60920=CARTESIAN_POINT('Ctrl Pts',(69.8239715224121,1.40255269618767,339.71601946475));
#60921=CARTESIAN_POINT('Ctrl Pts',(69.816210267486,1.53346488874996,339.675083949135));
#60922=CARTESIAN_POINT('Ctrl Pts',(69.8084490125598,1.66230779302521,339.628813656192));
#60923=CARTESIAN_POINT('Ctrl Pts',(69.8006753421551,1.7913568039575,339.582469345859));
#60924=CARTESIAN_POINT('Ctrl Pts',(69.7929016717505,1.91832954965948,339.530773352398));
#60925=CARTESIAN_POINT('Ctrl Pts',(69.7851280013458,2.04276542571683,339.473957138596));
#60926=CARTESIAN_POINT('Ctrl Pts',(69.7777161971688,2.16140878180525,339.419785733216));
#60927=CARTESIAN_POINT('Ctrl Pts',(69.7703043929917,2.27774587884159,339.360960202206));
#60928=CARTESIAN_POINT('Ctrl Pts',(69.7628925888147,2.39140137639818,339.297718292241));
#60929=CARTESIAN_POINT('Ctrl Pts',(69.7551175100363,2.5106274684532,339.23137670788));
#60930=CARTESIAN_POINT('Ctrl Pts',(69.7473424312578,2.62727922456917,339.159965226741));
#60931=CARTESIAN_POINT('Ctrl Pts',(69.7395673524794,2.74089549708878,339.083708478398));
#60932=CARTESIAN_POINT('Ctrl Pts',(69.7318018414304,2.85437195755189,339.007545568838));
#60933=CARTESIAN_POINT('Ctrl Pts',(69.7240363303814,2.96482004525852,338.926549471308));
#60934=CARTESIAN_POINT('Ctrl Pts',(69.7162708193324,3.0718027983208,338.840990839709));
#60935=CARTESIAN_POINT('Ctrl Pts',(69.7085130078102,3.17867947767189,338.755517039743));
#60936=CARTESIAN_POINT('Ctrl Pts',(69.700755196288,3.28209735669928,338.665489950814));
#60937=CARTESIAN_POINT('Ctrl Pts',(69.6929973847658,3.38164839624971,338.571223485956));
#60938=CARTESIAN_POINT('Ctrl Pts',(69.6852454112428,3.48112452048593,338.477027959601));
#60939=CARTESIAN_POINT('Ctrl Pts',(69.6774934377198,3.5767393146198,338.378599675055));
#60940=CARTESIAN_POINT('Ctrl Pts',(69.6697414641967,3.66811807531676,338.276292546162));
#60941=CARTESIAN_POINT('Ctrl Pts',(69.6619927736391,3.75945813705432,338.174028744398));
#60942=CARTESIAN_POINT('Ctrl Pts',(69.6542440830815,3.8465654735813,338.067889656402));
#60943=CARTESIAN_POINT('Ctrl Pts',(69.6464953925239,3.92910266577651,337.958265590559));
#60944=CARTESIAN_POINT('Ctrl Pts',(69.6387483141461,4.01162268541953,337.848664332919));
#60945=CARTESIAN_POINT('Ctrl Pts',(69.6310012357682,4.08957421709364,337.735579851731));
#60946=CARTESIAN_POINT('Ctrl Pts',(69.6232541573904,4.16266078838846,337.619434714459));
#60947=CARTESIAN_POINT('Ctrl Pts',(69.6155070140846,4.2357479722191,337.503288603779));
#60948=CARTESIAN_POINT('Ctrl Pts',(69.6077598707788,4.30396990616789,337.384082116675));
#60949=CARTESIAN_POINT('Ctrl Pts',(69.600012727473,4.36707425518542,337.262265570661));
#60950=CARTESIAN_POINT('Ctrl Pts',(69.5922638424449,4.43019279140031,337.140421637701));
#60951=CARTESIAN_POINT('Ctrl Pts',(69.5845149574168,4.48819127347767,337.015966825173));
#60952=CARTESIAN_POINT('Ctrl Pts',(69.5767660723887,4.54086418513642,336.889374371226));
#60953=CARTESIAN_POINT('Ctrl Pts',(69.569008962614,4.59359300436785,336.76264755074));
#60954=CARTESIAN_POINT('Ctrl Pts',(69.5612518528393,4.64098481115718,336.633778917917));
#60955=CARTESIAN_POINT('Ctrl Pts',(69.5534947430645,4.68288277218002,336.503260457978));
#60956=CARTESIAN_POINT('Ctrl Pts',(69.5457334881384,4.72480312213359,336.372672253146));
#60957=CARTESIAN_POINT('Ctrl Pts',(69.5379722332122,4.76122367286807,336.240432841153));
#60958=CARTESIAN_POINT('Ctrl Pts',(69.530210978286,4.79203828490623,336.107046583705));
#60959=CARTESIAN_POINT('Ctrl Pts',(69.5224373078814,4.82290219028119,335.973446951715));
#60960=CARTESIAN_POINT('Ctrl Pts',(69.5146636374767,4.84814216488861,335.838697192633));
#60961=CARTESIAN_POINT('Ctrl Pts',(69.5068899670721,4.86770359124532,335.703309896331));
#60962=CARTESIAN_POINT('Ctrl Pts',(69.499478162895,4.88635442849899,335.574224911244));
#60963=CARTESIAN_POINT('Ctrl Pts',(69.4920663587178,4.89984346311244,335.444560694164));
#60964=CARTESIAN_POINT('Ctrl Pts',(69.4846545545407,4.9081675030951,335.314761535231));
#60965=CARTESIAN_POINT('Ctrl Pts',(69.4768794757623,4.91689952907331,335.178600532868));
#60966=CARTESIAN_POINT('Ctrl Pts',(69.4691043969839,4.91997504979721,335.04186073246));
#60967=CARTESIAN_POINT('Ctrl Pts',(69.4613293182054,4.91733340760958,334.905051482862));
#60968=CARTESIAN_POINT('Ctrl Pts',(69.4535638071564,4.91469501613083,334.768410585754));
#60969=CARTESIAN_POINT('Ctrl Pts',(69.4457982961074,4.90635346750967,334.631700796567));
#60970=CARTESIAN_POINT('Ctrl Pts',(69.4380327850584,4.89229989523602,334.495436032228));
#60971=CARTESIAN_POINT('Ctrl Pts',(69.4302749735362,4.8782602571202,334.3593063748));
#60972=CARTESIAN_POINT('Ctrl Pts',(69.422517162014,4.85851990585494,334.22362125043));
#60973=CARTESIAN_POINT('Ctrl Pts',(69.4147593504918,4.83312200420676,334.0888936643));
#60974=CARTESIAN_POINT('Ctrl Pts',(69.4070073769688,4.80774321528501,333.954267464951));
#60975=CARTESIAN_POINT('Ctrl Pts',(69.3992554034458,4.77671542241618,333.82059775213));
#60976=CARTESIAN_POINT('Ctrl Pts',(69.3915034299228,4.74013346582818,333.688391144954));
#60977=CARTESIAN_POINT('Ctrl Pts',(69.3837547393651,4.7035670017205,333.556240527354));
#60978=CARTESIAN_POINT('Ctrl Pts',(69.3760060488075,4.66145115625928,333.425552158941));
#60979=CARTESIAN_POINT('Ctrl Pts',(69.3682573582499,4.61393155124512,333.296821000915));
#60980=CARTESIAN_POINT('Ctrl Pts',(69.3605102798721,4.56642183308168,333.168116626482));
#60981=CARTESIAN_POINT('Ctrl Pts',(69.3527632014942,4.51351072694607,333.041369018917));
#60982=CARTESIAN_POINT('Ctrl Pts',(69.3450161231164,4.45539314060015,332.917056163697));
#60983=CARTESIAN_POINT('Ctrl Pts',(69.3372689798106,4.39727506717287,332.792742266615));
#60984=CARTESIAN_POINT('Ctrl Pts',(69.3295218365048,4.33395059204179,332.670863516668));
#60985=CARTESIAN_POINT('Ctrl Pts',(69.321774693199,4.26566184383653,332.551875800427));
#60986=CARTESIAN_POINT('Ctrl Pts',(69.3140258081709,4.19735774287091,332.43286133322));
#60987=CARTESIAN_POINT('Ctrl Pts',(69.3062769231428,4.12408734249344,332.316739532024));
#60988=CARTESIAN_POINT('Ctrl Pts',(69.2985280381147,4.04613738210735,332.203939316178));
#60989=CARTESIAN_POINT('Ctrl Pts',(69.29077092834,3.96810468482788,332.091019373018));
#60990=CARTESIAN_POINT('Ctrl Pts',(69.2830138185653,3.88538272819031,331.981428379928));
#60991=CARTESIAN_POINT('Ctrl Pts',(69.2752567087905,3.79830036155177,331.875564462829));
#60992=CARTESIAN_POINT('Ctrl Pts',(69.2674954538644,3.71117146088084,331.769643975438));
#60993=CARTESIAN_POINT('Ctrl Pts',(69.2597341989382,3.61967776794487,331.667454823602));
#60994=CARTESIAN_POINT('Ctrl Pts',(69.251972944012,3.52418597310136,331.569359201331));
#60995=CARTESIAN_POINT('Ctrl Pts',(69.2441992736074,3.42854142250688,331.471106658033));
#60996=CARTESIAN_POINT('Ctrl Pts',(69.2364256032027,3.32888627386391,331.376960998336));
#60997=CARTESIAN_POINT('Ctrl Pts',(69.228651932798,3.22562201827858,331.287245543037));
#60998=CARTESIAN_POINT('Ctrl Pts',(69.2212401286209,3.12716473863469,331.201706363767));
#60999=CARTESIAN_POINT('Ctrl Pts',(69.2138283244439,3.02542702285736,331.120194398792));
#61000=CARTESIAN_POINT('Ctrl Pts',(69.2064165202668,2.92078075663575,331.042952763213));
#61001=CARTESIAN_POINT('Ctrl Pts',(69.1986414414883,2.8110054651814,330.961925284983));
#61002=CARTESIAN_POINT('Ctrl Pts',(69.1908663627099,2.69768239053949,330.885341261864));
#61003=CARTESIAN_POINT('Ctrl Pts',(69.1830912839315,2.5812070296896,330.813527340065));
#61004=CARTESIAN_POINT('Ctrl Pts',(69.1753257728825,2.46487499918649,330.74180178987));
#61005=CARTESIAN_POINT('Ctrl Pts',(69.1675602618335,2.34539873028618,330.674834864729));
#61006=CARTESIAN_POINT('Ctrl Pts',(69.1597947507845,2.22320558852179,330.61291213062));
#61007=CARTESIAN_POINT('Ctrl Pts',(69.1520369392623,2.10113360161322,330.551050793081));
#61008=CARTESIAN_POINT('Ctrl Pts',(69.14427912774,1.97635044904432,330.494223869195));
#61009=CARTESIAN_POINT('Ctrl Pts',(69.1365213162179,1.84931088566766,330.442672679009));
#61010=CARTESIAN_POINT('Ctrl Pts',(69.1287693426949,1.72236692359109,330.391160282729));
#61011=CARTESIAN_POINT('Ctrl Pts',(69.1210173691719,1.59317029126581,330.344915864127));
#61012=CARTESIAN_POINT('Ctrl Pts',(69.1132653956489,1.46219833900484,330.304133830707));
#61013=CARTESIAN_POINT('Ctrl Pts',(69.1055167050913,1.33128185344349,330.263369068502));
#61014=CARTESIAN_POINT('Ctrl Pts',(69.0977680145337,1.19859191574505,330.228062206407));
#61015=CARTESIAN_POINT('Ctrl Pts',(69.090019323976,1.06462355365488,330.19835863985));
#61016=CARTESIAN_POINT('Ctrl Pts',(69.0822722455982,0.930683064801266,330.168661253368));
#61017=CARTESIAN_POINT('Ctrl Pts',(69.0745251672204,0.795465061989936,330.144564928097));
#61018=CARTESIAN_POINT('Ctrl Pts',(69.0667780888426,0.659476969178747,330.12616442731));
#61019=CARTESIAN_POINT('Ctrl Pts',(69.0590309455368,0.523487736656453,330.107763772309));
#61020=CARTESIAN_POINT('Ctrl Pts',(69.051283802231,0.386728788605607,330.095059089417));
#61021=CARTESIAN_POINT('Ctrl Pts',(69.0435366589251,0.249714519465306,330.088093473887));
#61022=CARTESIAN_POINT('Ctrl Pts',(69.0357877738971,0.112669446608407,330.081126292339));
#61023=CARTESIAN_POINT('Ctrl Pts',(69.028038888869,-0.0246306712668604,
330.079900765477));
#61024=CARTESIAN_POINT('Ctrl Pts',(69.0202900038409,-0.161669975591024,
330.084407880886));
#61025=CARTESIAN_POINT('Ctrl Pts',(69.0125328940661,-0.298854734848679,
330.088919780194));
#61026=CARTESIAN_POINT('Ctrl Pts',(69.0047757842914,-0.43577773628084,330.099176463635));
#61027=CARTESIAN_POINT('Ctrl Pts',(68.9970186745167,-0.571926228050113,
330.11511684355));
#61028=CARTESIAN_POINT('Ctrl Pts',(68.9892574195905,-0.708147473220204,
330.131065741494));
#61029=CARTESIAN_POINT('Ctrl Pts',(68.9814961646644,-0.84359299826389,330.152704326145));
#61030=CARTESIAN_POINT('Ctrl Pts',(68.9737349097382,-0.977759789317654,
330.179920243721));
#61031=CARTESIAN_POINT('Ctrl Pts',(68.9659612393335,-1.11214120351225,330.207179697895));
#61032=CARTESIAN_POINT('Ctrl Pts',(68.9581875689289,-1.2452394164035,330.240034219899));
#61033=CARTESIAN_POINT('Ctrl Pts',(68.9504138985242,-1.37656527075809,330.278321154733));
#61034=CARTESIAN_POINT('Ctrl Pts',(68.9430020943471,-1.50177787499784,330.31482582354));
#61035=CARTESIAN_POINT('Ctrl Pts',(68.93559029017,-1.62537914104378,330.356268437812));
#61036=CARTESIAN_POINT('Ctrl Pts',(68.9281784859929,-1.74696337953491,330.402467834472));
#61037=CARTESIAN_POINT('Ctrl Pts',(68.9204034072145,-1.87450682373488,330.450931601183));
#61038=CARTESIAN_POINT('Ctrl Pts',(68.912628328436,-2.00023358078962,330.504783382991));
#61039=CARTESIAN_POINT('Ctrl Pts',(68.9048532496576,-2.1236549408234,330.563867365056));
#61040=CARTESIAN_POINT('Ctrl Pts',(68.8970877386086,-2.24692442301627,330.622878640519));
#61041=CARTESIAN_POINT('Ctrl Pts',(68.8893222275596,-2.3678938036929,330.687109138197));
#61042=CARTESIAN_POINT('Ctrl Pts',(68.8815567165105,-2.48609167231881,330.756354013431));
#61043=CARTESIAN_POINT('Ctrl Pts',(68.8737989049883,-2.60417234741377,330.825530232169));
#61044=CARTESIAN_POINT('Ctrl Pts',(68.8660410934661,-2.71948664397022,330.899710738053));
#61045=CARTESIAN_POINT('Ctrl Pts',(68.8582832819439,-2.83158553686556,330.97864371015));
#61046=CARTESIAN_POINT('Ctrl Pts',(68.8505313084209,-2.94360007178898,331.057517282683));
#61047=CARTESIAN_POINT('Ctrl Pts',(68.8427793348979,-3.05240370102488,331.141135978685));
#61048=CARTESIAN_POINT('Ctrl Pts',(68.8350273613749,-3.15757462151169,331.229203589149));
#61049=CARTESIAN_POINT('Ctrl Pts',(68.8272786708173,-3.26270100205136,331.317233902928));
#61050=CARTESIAN_POINT('Ctrl Pts',(68.8195299802597,-3.36419743466158,331.409709133368));
#61051=CARTESIAN_POINT('Ctrl Pts',(68.811781289702,-3.46167376530756,331.506291682885));
#61052=CARTESIAN_POINT('Ctrl Pts',(68.8040342113242,-3.55912981518887,331.602854137596));
#61053=CARTESIAN_POINT('Ctrl Pts',(68.7962871329463,-3.65256714931052,331.703521936658));
#61054=CARTESIAN_POINT('Ctrl Pts',(68.7885400545685,-3.7416314829952,331.807919658286));
#61055=CARTESIAN_POINT('Ctrl Pts',(68.7807929112627,-3.83069656312466,331.912318254866));
#61056=CARTESIAN_POINT('Ctrl Pts',(68.7730457679569,-3.91538831602784,332.020446538999));
#61057=CARTESIAN_POINT('Ctrl Pts',(68.7652986246511,-3.9953921336405,332.131895266741));
#61058=CARTESIAN_POINT('Ctrl Pts',(68.757549739623,-4.07541393780995,332.243369050522));
#61059=CARTESIAN_POINT('Ctrl Pts',(68.7498008545949,-4.15074548155537,332.358164445908));
#61060=CARTESIAN_POINT('Ctrl Pts',(68.7420519695668,-4.2211151829362,332.475842779285));
#61061=CARTESIAN_POINT('Ctrl Pts',(68.734294859792,-4.29155957544508,332.593646017662));
#61062=CARTESIAN_POINT('Ctrl Pts',(68.7265377500173,-4.35703140423779,332.714337970629));
#61063=CARTESIAN_POINT('Ctrl Pts',(68.7187806402426,-4.41730455978964,332.837454396189));
#61064=CARTESIAN_POINT('Ctrl Pts',(68.7110193853164,-4.47760992338861,332.960636611231));
#61065=CARTESIAN_POINT('Ctrl Pts',(68.7032581303902,-4.53271092138012,333.08624552262));
#61066=CARTESIAN_POINT('Ctrl Pts',(68.6954968754641,-4.58242982479273,333.213797334189));
#61067=CARTESIAN_POINT('Ctrl Pts',(68.6877232050594,-4.63222826224748,333.341553187088));
#61068=CARTESIAN_POINT('Ctrl Pts',(68.6799495346548,-4.67662727394311,333.471257780882));
#61069=CARTESIAN_POINT('Ctrl Pts',(68.6721758642501,-4.71549892889219,333.602411750866));
#61070=CARTESIAN_POINT('Ctrl Pts',(68.664764060073,-4.75256109895122,333.727460471993));
#61071=CARTESIAN_POINT('Ctrl Pts',(68.657352255896,-4.78459885776639,333.853826390087));
#61072=CARTESIAN_POINT('Ctrl Pts',(68.6499404517189,-4.81154500744351,333.981070314572));
#61073=CARTESIAN_POINT('Ctrl Pts',(68.639026225491,-4.85122446557838,334.168442908989));
#61074=CARTESIAN_POINT('Ctrl Pts',(68.6281119992631,-4.87997008721691,334.35820527783));
#61075=CARTESIAN_POINT('Ctrl Pts',(68.6171977730352,-4.89755553794552,334.549297420421));
#61076=CARTESIAN_POINT('Ctrl Pts',(68.6087376408596,-4.91118685128135,334.697421964504));
#61077=CARTESIAN_POINT('Ctrl Pts',(68.6002775086841,-4.91811336021633,334.846345332992));
#61078=CARTESIAN_POINT('Ctrl Pts',(68.5918173765086,-4.91824799793813,334.995562289148));
#61079=CARTESIAN_POINT('',(66.8418173765624,-4.91824999982528,334.99995854384));
#61080=CARTESIAN_POINT('Ctrl Pts',(68.5918173764684,-4.91824799793877,334.995562289857));
#61081=CARTESIAN_POINT('Ctrl Pts',(68.5841669567107,-4.91836974957348,335.130497811652));
#61082=CARTESIAN_POINT('Ctrl Pts',(68.5765165369531,-4.91293425515066,335.265607840655));
#61083=CARTESIAN_POINT('Ctrl Pts',(68.5688661171954,-4.90192521624238,335.400390105856));
#61084=CARTESIAN_POINT('Ctrl Pts',(68.5612218503107,-4.89092503138647,335.535063972017));
#61085=CARTESIAN_POINT('Ctrl Pts',(68.553577583426,-4.87436025167078,335.669410199118));
#61086=CARTESIAN_POINT('Ctrl Pts',(68.5459333165412,-4.85226664415567,335.802926818903));
#61087=CARTESIAN_POINT('Ctrl Pts',(68.5382926658293,-4.83018348817305,335.936380277736));
#61088=CARTESIAN_POINT('Ctrl Pts',(68.5306520151174,-4.80257676992838,336.069004512944));
#61089=CARTESIAN_POINT('Ctrl Pts',(68.5230113644055,-4.76953402762972,336.200303387391));
#61090=CARTESIAN_POINT('Ctrl Pts',(68.5153724381459,-4.73649874289362,336.331572628415));
#61091=CARTESIAN_POINT('Ctrl Pts',(68.5077335118862,-4.69802997143603,336.461516712868));
#61092=CARTESIAN_POINT('Ctrl Pts',(68.5000945856265,-4.65426610759358,336.589650924639));
#61093=CARTESIAN_POINT('Ctrl Pts',(68.4924556208709,-4.61050202320521,336.717785782136));
#61094=CARTESIAN_POINT('Ctrl Pts',(68.4848166561152,-4.56144292382961,336.844110367576));
#61095=CARTESIAN_POINT('Ctrl Pts',(68.4771776913595,-4.50727651927473,336.968156863996));
#61096=CARTESIAN_POINT('Ctrl Pts',(68.4695369253401,-4.45309734231094,337.092232610513));
#61097=CARTESIAN_POINT('Ctrl Pts',(68.4618961593207,-4.39380862705637,337.214028830905));
#61098=CARTESIAN_POINT('Ctrl Pts',(68.4542553933013,-4.32964525353834,337.333099878062));
#61099=CARTESIAN_POINT('Ctrl Pts',(68.4466066995075,-4.26541530649257,337.452294468905));
#61100=CARTESIAN_POINT('Ctrl Pts',(68.4389580057136,-4.19630079483433,337.568757886408));
#61101=CARTESIAN_POINT('Ctrl Pts',(68.4313093119198,-4.12258153727244,337.682070940717));
#61102=CARTESIAN_POINT('Ctrl Pts',(68.4236562563777,-4.0488202405258,337.795448612992));
#61103=CARTESIAN_POINT('Ctrl Pts',(68.4160032008355,-3.97044920342802,337.905672018035));
#61104=CARTESIAN_POINT('Ctrl Pts',(68.4083501452933,-3.88778939609991,338.012354008757));
#61105=CARTESIAN_POINT('Ctrl Pts',(68.4006857519601,-3.80500713054283,338.119194045911));
#61106=CARTESIAN_POINT('Ctrl Pts',(68.3930213586268,-3.71792366853709,338.222481886915));
#61107=CARTESIAN_POINT('Ctrl Pts',(68.3853569652935,-3.6268980684741,338.321865961083));
#61108=CARTESIAN_POINT('Ctrl Pts',(68.3808054493441,-3.57284232622804,338.38088540059));
#61109=CARTESIAN_POINT('Ctrl Pts',(68.3762539333946,-3.51739702621145,338.43852886839));
#61110=CARTESIAN_POINT('Ctrl Pts',(68.3717024174451,-3.46064280031056,338.494729527611));
#61111=CARTESIAN_POINT('Ctrl Pts',(68.3639273386667,-3.36369299670928,338.590733706811));
#61112=CARTESIAN_POINT('Ctrl Pts',(68.3561522598883,-3.26259198530339,338.682852202978));
#61113=CARTESIAN_POINT('Ctrl Pts',(68.3483771811098,-3.15768405087805,338.770704774618));
#61114=CARTESIAN_POINT('Ctrl Pts',(68.3406116700608,-3.05290521234471,338.858449238076));
#61115=CARTESIAN_POINT('Ctrl Pts',(68.3328461590118,-2.94432906873354,338.941937973434));
#61116=CARTESIAN_POINT('Ctrl Pts',(68.3250806479628,-2.83233736183333,339.020826796974));
#61117=CARTESIAN_POINT('Ctrl Pts',(68.3173228364406,-2.72045669503679,339.099637402015));
#61118=CARTESIAN_POINT('Ctrl Pts',(68.3095650249184,-2.60516752185295,339.173856947891));
#61119=CARTESIAN_POINT('Ctrl Pts',(68.3018072133962,-2.48688506491217,339.243181086923));
#61120=CARTESIAN_POINT('Ctrl Pts',(68.2940552398732,-2.3686916192711,339.312453057341));
#61121=CARTESIAN_POINT('Ctrl Pts',(68.2863032663502,-2.24750970931159,339.376836756789));
#61122=CARTESIAN_POINT('Ctrl Pts',(68.2785512928272,-2.12378367906824,339.436071003379));
#61123=CARTESIAN_POINT('Ctrl Pts',(68.2708026022696,-2.00011004687207,339.495280164231));
#61124=CARTESIAN_POINT('Ctrl Pts',(68.263053911712,-1.87389478915699,339.549344041241));
#61125=CARTESIAN_POINT('Ctrl Pts',(68.2553052211544,-1.74560680731257,339.598047404797));
#61126=CARTESIAN_POINT('Ctrl Pts',(68.2475581427765,-1.61734551685426,339.646740635212));
#61127=CARTESIAN_POINT('Ctrl Pts',(68.2398110643987,-1.48701272524551,339.690075431939));
#61128=CARTESIAN_POINT('Ctrl Pts',(68.2320639860209,-1.35509689867547,339.727884882027));
#61129=CARTESIAN_POINT('Ctrl Pts',(68.2243168427151,-1.22317996652401,339.765694648995));
#61130=CARTESIAN_POINT('Ctrl Pts',(68.2165696994093,-1.08968034869367,339.797978869266));
#61131=CARTESIAN_POINT('Ctrl Pts',(68.2088225561035,-0.955100856407698,
339.824620753654));
#61132=CARTESIAN_POINT('Ctrl Pts',(68.2010736710754,-0.820491107794473,
339.851268627704));
#61133=CARTESIAN_POINT('Ctrl Pts',(68.1933247860473,-0.684801384981352,
339.872271565774));
#61134=CARTESIAN_POINT('Ctrl Pts',(68.1855759010192,-0.548543458744524,
339.887564131177));
#61135=CARTESIAN_POINT('Ctrl Pts',(68.1778187912445,-0.41214090693698,339.902872928267));
#61136=CARTESIAN_POINT('Ctrl Pts',(68.1700616814697,-0.275169336012001,
339.912459201514));
#61137=CARTESIAN_POINT('Ctrl Pts',(68.162304571695,-0.138144948494133,339.916309493482));
#61138=CARTESIAN_POINT('Ctrl Pts',(68.1545433167688,-0.00104733952457867,
339.920161842924));
#61139=CARTESIAN_POINT('Ctrl Pts',(68.1467820618427,0.136102751636794,339.918272108931));
#61140=CARTESIAN_POINT('Ctrl Pts',(68.1390208069165,0.272791369337971,339.910678968464));
#61141=CARTESIAN_POINT('Ctrl Pts',(68.1312471365118,0.409698644280568,339.903073681447));
#61142=CARTESIAN_POINT('Ctrl Pts',(68.1234734661072,0.546142581378811,339.889746794335));
#61143=CARTESIAN_POINT('Ctrl Pts',(68.1156997957025,0.681615686580704,339.870788757307));
#61144=CARTESIAN_POINT('Ctrl Pts',(68.1082879915253,0.810782486143793,339.852713221464));
#61145=CARTESIAN_POINT('Ctrl Pts',(68.1008761873482,0.939066521009833,339.82951904882));
#61146=CARTESIAN_POINT('Ctrl Pts',(68.093464383171,1.0660402256666,339.801327035285));
#61147=CARTESIAN_POINT('Ctrl Pts',(68.0856893043926,1.1992372898225,339.771753247187));
#61148=CARTESIAN_POINT('Ctrl Pts',(68.0779142256141,1.33141325695796,339.736585853835));
#61149=CARTESIAN_POINT('Ctrl Pts',(68.0701391468357,1.46206206163609,339.695908601157));
#61150=CARTESIAN_POINT('Ctrl Pts',(68.0623736357867,1.59255009464246,339.655281404429));
#61151=CARTESIAN_POINT('Ctrl Pts',(68.0546081247376,1.72151433476501,339.609157954181));
#61152=CARTESIAN_POINT('Ctrl Pts',(68.0468426136886,1.8484587681849,339.557673007667));
#61153=CARTESIAN_POINT('Ctrl Pts',(68.0390848021664,1.97527733582913,339.506239108628));
#61154=CARTESIAN_POINT('Ctrl Pts',(68.0313269906443,2.10007972226158,339.449454438301));
#61155=CARTESIAN_POINT('Ctrl Pts',(68.0235691791221,2.22238529423551,339.387503466263));
#61156=CARTESIAN_POINT('Ctrl Pts',(68.0158172055991,2.34459882738826,339.325599114295));
#61157=CARTESIAN_POINT('Ctrl Pts',(68.0080652320761,2.4643189387153,339.258536375014));
#61158=CARTESIAN_POINT('Ctrl Pts',(68.0003132585531,2.58108553474316,339.186547566294));
#61159=CARTESIAN_POINT('Ctrl Pts',(67.9925645679955,2.69780268004835,339.114589244877));
#61160=CARTESIAN_POINT('Ctrl Pts',(67.9848158774378,2.81156846580788,339.037709208014));
#61161=CARTESIAN_POINT('Ctrl Pts',(67.9770671868802,2.9219481514017,338.956185291796));
#61162=CARTESIAN_POINT('Ctrl Pts',(67.9693201085024,3.03230487158003,338.874678337309));
#61163=CARTESIAN_POINT('Ctrl Pts',(67.9615730301245,3.13927657868824,338.788529657376));
#61164=CARTESIAN_POINT('Ctrl Pts',(67.9538259517467,3.24245857498245,338.698059687461));
#61165=CARTESIAN_POINT('Ctrl Pts',(67.9460788084408,3.34564143604117,338.60758895932));
#61166=CARTESIAN_POINT('Ctrl Pts',(67.938331665135,3.44503422903476,338.512797126654));
#61167=CARTESIAN_POINT('Ctrl Pts',(67.9305845218292,3.54026664344243,338.414043812816));
#61168=CARTESIAN_POINT('Ctrl Pts',(67.9228356368011,3.63552046811895,338.315268297137));
#61169=CARTESIAN_POINT('Ctrl Pts',(67.915086751773,3.72661178170897,338.212529809348));
#61170=CARTESIAN_POINT('Ctrl Pts',(67.9073378667448,3.81320860857434,338.106223296866));
#61171=CARTESIAN_POINT('Ctrl Pts',(67.8995807569701,3.89989735020622,337.999803949554));
#61172=CARTESIAN_POINT('Ctrl Pts',(67.8918236471954,3.98208182834817,337.889809315917));
#61173=CARTESIAN_POINT('Ctrl Pts',(67.8840665374206,4.05947137955017,337.77666619908));
#61174=CARTESIAN_POINT('Ctrl Pts',(67.8763052824944,4.13690228525394,337.663462622179));
#61175=CARTESIAN_POINT('Ctrl Pts',(67.8685440275683,4.20953295162168,337.547107541056));
#61176=CARTESIAN_POINT('Ctrl Pts',(67.8607827726421,4.27711777203967,337.428054082306));
#61177=CARTESIAN_POINT('Ctrl Pts',(67.8530091022375,4.34481070614445,337.308810176822));
#61178=CARTESIAN_POINT('Ctrl Pts',(67.8452354318327,4.40744148597028,337.186859615899));
#61179=CARTESIAN_POINT('Ctrl Pts',(67.8374617614281,4.46481153885143,337.062678109895));
#61180=CARTESIAN_POINT('Ctrl Pts',(67.830049957251,4.51951100196802,336.944277282873));
#61181=CARTESIAN_POINT('Ctrl Pts',(67.8226381530741,4.56942837956783,336.823848803438));
#61182=CARTESIAN_POINT('Ctrl Pts',(67.815226348897,4.6144338712744,336.701817590148));
#61183=CARTESIAN_POINT('Ctrl Pts',(67.8074512701186,4.66164521619439,336.573805263581));
#61184=CARTESIAN_POINT('Ctrl Pts',(67.7996761913402,4.70360020493318,336.443624578518));
#61185=CARTESIAN_POINT('Ctrl Pts',(67.7919011125617,4.74009540018406,336.31174641591));
#61186=CARTESIAN_POINT('Ctrl Pts',(67.7841356015127,4.77654568577369,336.180030537778));
#61187=CARTESIAN_POINT('Ctrl Pts',(67.7763700904637,4.80754944275621,336.046621711435));
#61188=CARTESIAN_POINT('Ctrl Pts',(67.7686045794148,4.83295156984315,335.912009970368));
#61189=CARTESIAN_POINT('Ctrl Pts',(67.7608467678926,4.8583285106471,335.777531697234));
#61190=CARTESIAN_POINT('Ctrl Pts',(67.7530889563704,4.87811480237946,335.641853264523));
#61191=CARTESIAN_POINT('Ctrl Pts',(67.7453311448482,4.89220547121353,335.505478674059));
#61192=CARTESIAN_POINT('Ctrl Pts',(67.7375791713252,4.90628553637245,335.369206709799));
#61193=CARTESIAN_POINT('Ctrl Pts',(67.7298271978023,4.91467846996816,335.232240017784));
#61194=CARTESIAN_POINT('Ctrl Pts',(67.7220752242793,4.91733065007793,335.095091220963));
#61195=CARTESIAN_POINT('Ctrl Pts',(67.7143265337216,4.91998170698785,334.958000506738));
#61196=CARTESIAN_POINT('Ctrl Pts',(67.706577843164,4.91689683838061,334.820728231084));
#61197=CARTESIAN_POINT('Ctrl Pts',(67.6988291526064,4.90807441945593,334.683790329714));
#61198=CARTESIAN_POINT('Ctrl Pts',(67.6910820742286,4.8992538361092,334.546880919418));
#61199=CARTESIAN_POINT('Ctrl Pts',(67.6833349958508,4.88469810200353,334.410306134847));
#61200=CARTESIAN_POINT('Ctrl Pts',(67.675587917473,4.86445767298652,334.274579700985));
#61201=CARTESIAN_POINT('Ctrl Pts',(67.6678407741671,4.84421707433522,334.138852129605));
#61202=CARTESIAN_POINT('Ctrl Pts',(67.6600936308613,4.81829174339686,334.003973309714));
#61203=CARTESIAN_POINT('Ctrl Pts',(67.6523464875555,4.78678369885221,333.870449256163));
#61204=CARTESIAN_POINT('Ctrl Pts',(67.6445976025274,4.75526857063036,333.73689518357));
#61205=CARTESIAN_POINT('Ctrl Pts',(67.6368487174994,4.7181683210212,333.604696863749));
#61206=CARTESIAN_POINT('Ctrl Pts',(67.6290998324713,4.67563541866781,333.474347190807));
#61207=CARTESIAN_POINT('Ctrl Pts',(67.6213427226966,4.63305737145227,333.343859163374));
#61208=CARTESIAN_POINT('Ctrl Pts',(67.6135856129219,4.58503527426134,333.215224074624));
#61209=CARTESIAN_POINT('Ctrl Pts',(67.6058285031472,4.53177074027741,333.088917317313));
#61210=CARTESIAN_POINT('Ctrl Pts',(67.598067248221,4.47847774342953,332.96254306571));
#61211=CARTESIAN_POINT('Ctrl Pts',(67.5903059932948,4.41993689450501,332.838499978005));
#61212=CARTESIAN_POINT('Ctrl Pts',(67.5825447383686,4.35639632549274,332.717239802841));
#61213=CARTESIAN_POINT('Ctrl Pts',(67.574771067964,4.29275411227796,332.595785650916));
#61214=CARTESIAN_POINT('Ctrl Pts',(67.5669973975593,4.22409639261416,332.477123645954));
#61215=CARTESIAN_POINT('Ctrl Pts',(67.5592237271547,4.15071574242629,332.361678206118));
#61216=CARTESIAN_POINT('Ctrl Pts',(67.5518119229775,4.08075097915844,332.251606779279));
#61217=CARTESIAN_POINT('Ctrl Pts',(67.5444001188004,4.0064932588492,332.144459431106));
#61218=CARTESIAN_POINT('Ctrl Pts',(67.5369883146232,3.92822966214747,332.040575261318));
#61219=CARTESIAN_POINT('Ctrl Pts',(67.5292132358448,3.84613013343676,331.931599418913));
#61220=CARTESIAN_POINT('Ctrl Pts',(67.5214381570663,3.75936266986788,331.825870335359));
#61221=CARTESIAN_POINT('Ctrl Pts',(67.5136630782879,3.66821315367794,331.723813906127));
#61222=CARTESIAN_POINT('Ctrl Pts',(67.5058975672389,3.5771758027706,331.621883063829));
#61223=CARTESIAN_POINT('Ctrl Pts',(67.4981320561899,3.48176738644495,331.523616172215));
#61224=CARTESIAN_POINT('Ctrl Pts',(67.4903665451409,3.38231605010601,331.429408844506));
#61225=CARTESIAN_POINT('Ctrl Pts',(67.4826087336187,3.28296332005659,331.335294923635));
#61226=CARTESIAN_POINT('Ctrl Pts',(67.4748509220965,3.1795759292109,331.245232823629));
#61227=CARTESIAN_POINT('Ctrl Pts',(67.4670931105743,3.07252089609362,331.159583563522));
#61228=CARTESIAN_POINT('Ctrl Pts',(67.4593411370513,2.96554642528396,331.0739987572));
#61229=CARTESIAN_POINT('Ctrl Pts',(67.4515891635283,2.85491010986719,330.992820424088));
#61230=CARTESIAN_POINT('Ctrl Pts',(67.4438371900053,2.74101400751839,330.916371065696));
#61231=CARTESIAN_POINT('Ctrl Pts',(67.4360884994476,2.62716614023639,330.839954083652));
#61232=CARTESIAN_POINT('Ctrl Pts',(67.4283398088901,2.51006155565071,330.768262310439));
#61233=CARTESIAN_POINT('Ctrl Pts',(67.4205911183325,2.39013323583607,330.701576314804));
#61234=CARTESIAN_POINT('Ctrl Pts',(67.4128440399546,2.27022986810987,330.634904193748));
#61235=CARTESIAN_POINT('Ctrl Pts',(67.4050969615767,2.1475042751367,330.5732359685));
#61236=CARTESIAN_POINT('Ctrl Pts',(67.3973498831989,2.02241576376905,330.516807215727));
#61237=CARTESIAN_POINT('Ctrl Pts',(67.3896027398931,1.89732620403919,330.460377990027));
#61238=CARTESIAN_POINT('Ctrl Pts',(67.3818555965873,1.76987404271365,330.409188485118));
#61239=CARTESIAN_POINT('Ctrl Pts',(67.3741084532814,1.64054000663724,330.363426744985));
#61240=CARTESIAN_POINT('Ctrl Pts',(67.3663595682533,1.51117689352342,330.317654716641));
#61241=CARTESIAN_POINT('Ctrl Pts',(67.3586106832252,1.37993143218229,330.277313011643));
#61242=CARTESIAN_POINT('Ctrl Pts',(67.3508617981971,1.24730061731481,330.24254014914));
#61243=CARTESIAN_POINT('Ctrl Pts',(67.3431046884224,1.11452902673065,330.207730378361));
#61244=CARTESIAN_POINT('Ctrl Pts',(67.3353475786476,0.980369523993994,330.178501356793));
#61245=CARTESIAN_POINT('Ctrl Pts',(67.3275904688729,0.845330981477995,330.154940805908));
#61246=CARTESIAN_POINT('Ctrl Pts',(67.3198292139467,0.710220278682479,330.131367665018));
#61247=CARTESIAN_POINT('Ctrl Pts',(67.3120679590206,0.574229987462297,330.113469081445));
#61248=CARTESIAN_POINT('Ctrl Pts',(67.3043067040944,0.437874271345128,330.101280862818));
#61249=CARTESIAN_POINT('Ctrl Pts',(67.2965330336897,0.301300430520302,330.089073147013));
#61250=CARTESIAN_POINT('Ctrl Pts',(67.2887593632851,0.164360387315896,330.082594068517));
#61251=CARTESIAN_POINT('Ctrl Pts',(67.2809856928804,0.0275693736396244,
330.081827271014));
#61252=CARTESIAN_POINT('Ctrl Pts',(67.2735738887033,-0.102853985439723,
330.08109616812));
#61253=CARTESIAN_POINT('Ctrl Pts',(67.2661620845263,-0.233141589771978,
330.085557491137));
#61254=CARTESIAN_POINT('Ctrl Pts',(67.2587502803492,-0.362852927357058,
330.095153334139));
#61255=CARTESIAN_POINT('Ctrl Pts',(67.2509752015708,-0.498921803987518,
330.105219497991));
#61256=CARTESIAN_POINT('Ctrl Pts',(67.2432001227923,-0.634786499232371,
330.120968035364));
#61257=CARTESIAN_POINT('Ctrl Pts',(67.2354250440139,-0.769934161220083,
330.142389018264));
#61258=CARTESIAN_POINT('Ctrl Pts',(67.2276595329649,-0.90491551540598,330.16378364128));
#61259=CARTESIAN_POINT('Ctrl Pts',(67.2198940219159,-1.03918120960381,330.190836760412));
#61260=CARTESIAN_POINT('Ctrl Pts',(67.2121285108669,-1.17222098590981,330.223486520202));
#61261=CARTESIAN_POINT('Ctrl Pts',(67.2043706993447,-1.30512885289008,330.25610390766));
#61262=CARTESIAN_POINT('Ctrl Pts',(67.1966128878225,-1.43681284373003,330.294306800219));
#61263=CARTESIAN_POINT('Ctrl Pts',(67.1888550763003,-1.56677075503651,330.337981932289));
#61264=CARTESIAN_POINT('Ctrl Pts',(67.1811031027773,-1.69663086889336,330.381624197437));
#61265=CARTESIAN_POINT('Ctrl Pts',(67.1733511292543,-1.82476711965399,330.430730381335));
#61266=CARTESIAN_POINT('Ctrl Pts',(67.1655991557313,-1.95069073243961,330.485136909177));
#61267=CARTESIAN_POINT('Ctrl Pts',(67.1578504651737,-2.0765610165007,330.539520395823));
#61268=CARTESIAN_POINT('Ctrl Pts',(67.1501017746161,-2.2002201682515,330.599199607159));
#61269=CARTESIAN_POINT('Ctrl Pts',(67.1423530840585,-2.32119794000141,330.66396227117));
#61270=CARTESIAN_POINT('Ctrl Pts',(67.1346060056806,-2.44215054131556,330.728711460769));
#61271=CARTESIAN_POINT('Ctrl Pts',(67.1268589273028,-2.56042252791154,330.798541814932));
#61272=CARTESIAN_POINT('Ctrl Pts',(67.119111848925,-2.67556724105116,330.873194576781));
#61273=CARTESIAN_POINT('Ctrl Pts',(67.1113647056192,-2.79071291921383,330.947847964291));
#61274=CARTESIAN_POINT('Ctrl Pts',(67.1036175623134,-2.90273094366841,331.027323627463));
#61275=CARTESIAN_POINT('Ctrl Pts',(67.0958704190076,-3.01120303533603,331.111319074225));
#61276=CARTESIAN_POINT('Ctrl Pts',(67.0881215339795,-3.11969951383285,331.195333404948));
#61277=CARTESIAN_POINT('Ctrl Pts',(67.0803726489515,-3.22464816421217,331.283869302008));
#61278=CARTESIAN_POINT('Ctrl Pts',(67.0726237639234,-3.32566355041658,331.376583792616));
#61279=CARTESIAN_POINT('Ctrl Pts',(67.0648666541487,-3.42678615539579,331.469396691344));
#61280=CARTESIAN_POINT('Ctrl Pts',(67.057109544374,-3.52396686820781,331.566396778631));
#61281=CARTESIAN_POINT('Ctrl Pts',(67.0493524345993,-3.61685654195464,331.667203603966));
#61282=CARTESIAN_POINT('Ctrl Pts',(67.0415911796731,-3.70979585297302,331.768064297245));
#61283=CARTESIAN_POINT('Ctrl Pts',(67.033829924747,-3.79843930344952,331.872735483765));
#61284=CARTESIAN_POINT('Ctrl Pts',(67.0260686698208,-3.88247853859796,331.98080417001));
#61285=CARTESIAN_POINT('Ctrl Pts',(67.0182949994162,-3.96665220913432,332.089045730934));
#61286=CARTESIAN_POINT('Ctrl Pts',(67.0105213290115,-4.04620671946224,332.200695333609));
#61287=CARTESIAN_POINT('Ctrl Pts',(67.0027476586069,-4.12087700240813,332.31531085719));
#61288=CARTESIAN_POINT('Ctrl Pts',(66.9953358544297,-4.19207136571891,332.424591000574));
#61289=CARTESIAN_POINT('Ctrl Pts',(66.9879240502525,-4.25882584262179,332.536566904497));
#61290=CARTESIAN_POINT('Ctrl Pts',(66.9805122460754,-4.32095074112603,332.650836796801));
#61291=CARTESIAN_POINT('Ctrl Pts',(66.9723313631025,-4.38952197050791,332.776963795562));
#61292=CARTESIAN_POINT('Ctrl Pts',(66.9641504801296,-4.45265114831385,332.906249954941));
#61293=CARTESIAN_POINT('Ctrl Pts',(66.9559695971568,-4.51005161674404,333.03821064413));
#61294=CARTESIAN_POINT('Ctrl Pts',(66.9478028851898,-4.56735265551854,333.169942749717));
#61295=CARTESIAN_POINT('Ctrl Pts',(66.9396361732229,-4.61894462767693,333.304339851162));
#61296=CARTESIAN_POINT('Ctrl Pts',(66.9314694612559,-4.66458640569054,333.440892330098));
#61297=CARTESIAN_POINT('Ctrl Pts',(66.9233215262709,-4.71012324369306,333.577130846273));
#61298=CARTESIAN_POINT('Ctrl Pts',(66.915173591286,-4.74973706429885,333.715514544774));
#61299=CARTESIAN_POINT('Ctrl Pts',(66.9070256563011,-4.78323481655576,333.855514197472));
#61300=CARTESIAN_POINT('Ctrl Pts',(66.8988889033995,-4.81668659708359,333.995321717096));
#61301=CARTESIAN_POINT('Ctrl Pts',(66.8907521504979,-4.84403895453746,334.136740452318));
#61302=CARTESIAN_POINT('Ctrl Pts',(66.8826153975964,-4.8651481098123,334.279224770064));
#61303=CARTESIAN_POINT('Ctrl Pts',(66.8744933613299,-4.88621908576203,334.42145138185));
#61304=CARTESIAN_POINT('Ctrl Pts',(66.8663713250634,-4.90106932749512,334.564739406573));
#61305=CARTESIAN_POINT('Ctrl Pts',(66.8582492887969,-4.90960585533241,334.708532321199));
#61306=CARTESIAN_POINT('Ctrl Pts',(66.8527719847366,-4.91536268244443,334.805502771623));
#61307=CARTESIAN_POINT('Ctrl Pts',(66.8472946806764,-4.91824918003111,334.902702554081));
#61308=CARTESIAN_POINT('Ctrl Pts',(66.8418173766161,-4.91824999982527,334.999958542886));
#61309=CARTESIAN_POINT('',(65.0918173765437,-4.91824798275492,335.004454506388));
#61310=CARTESIAN_POINT('Ctrl Pts',(66.8418173765086,-4.91824999982529,334.999958544795));
#61311=CARTESIAN_POINT('Ctrl Pts',(66.8337075228607,-4.91825121358016,335.143958554091));
#61312=CARTESIAN_POINT('Ctrl Pts',(66.8255976692128,-4.91192391682476,335.287838366001));
#61313=CARTESIAN_POINT('Ctrl Pts',(66.8174878155649,-4.89932552419494,335.431036507122));
#61314=CARTESIAN_POINT('Ctrl Pts',(66.8093674890112,-4.88671086224822,335.574419571511));
#61315=CARTESIAN_POINT('Ctrl Pts',(66.8012471624575,-4.8678089743011,335.717118876131));
#61316=CARTESIAN_POINT('Ctrl Pts',(66.7931268359039,-4.84272869959005,335.858581274351));
#61317=CARTESIAN_POINT('Ctrl Pts',(66.7849875446338,-4.81758985084326,336.000374052668));
#61318=CARTESIAN_POINT('Ctrl Pts',(66.7768482533637,-4.78624382425322,336.140923818903));
#61319=CARTESIAN_POINT('Ctrl Pts',(66.7687089620936,-4.7488503026307,336.279688972252));
#61320=CARTESIAN_POINT('Ctrl Pts',(66.7605596816537,-4.71141088877714,336.418624428964));
#61321=CARTESIAN_POINT('Ctrl Pts',(66.7524104012138,-4.66790926918605,336.555770583816));
#61322=CARTESIAN_POINT('Ctrl Pts',(66.744261120774,-4.61855401257615,336.690604003135));
#61323=CARTESIAN_POINT('Ctrl Pts',(66.7360932410512,-4.56908611137316,336.825745155748));
#61324=CARTESIAN_POINT('Ctrl Pts',(66.7279253613285,-4.51373798764962,336.958562709231));
#61325=CARTESIAN_POINT('Ctrl Pts',(66.7197574816058,-4.45276583261537,337.08855440494));
#61326=CARTESIAN_POINT('Ctrl Pts',(66.7139297250043,-4.40926239095552,337.18130307271));
#61327=CARTESIAN_POINT('Ctrl Pts',(66.7081019684029,-4.36289685369238,337.272613669177));
#61328=CARTESIAN_POINT('Ctrl Pts',(66.7022742118015,-4.31377583689369,337.362312657447));
#61329=CARTESIAN_POINT('Ctrl Pts',(66.6944991330231,-4.24824122359254,337.481984213389));
#61330=CARTESIAN_POINT('Ctrl Pts',(66.6867240542447,-4.17761943773648,337.599115742901));
#61331=CARTESIAN_POINT('Ctrl Pts',(66.6789489754663,-4.10213198839238,337.713244591316));
#61332=CARTESIAN_POINT('Ctrl Pts',(66.6711834644173,-4.02673743116046,337.827232996918));
#61333=CARTESIAN_POINT('Ctrl Pts',(66.6634179533682,-3.94648933743772,337.938225750497));
#61334=CARTESIAN_POINT('Ctrl Pts',(66.6556524423192,-3.86165540296115,338.045784071677));
#61335=CARTESIAN_POINT('Ctrl Pts',(66.647894630797,-3.77690558157742,338.153235748468));
#61336=CARTESIAN_POINT('Ctrl Pts',(66.6401368192748,-3.68757920847924,338.257259464575));
#61337=CARTESIAN_POINT('Ctrl Pts',(66.6323790077526,-3.59398743294007,338.357445069449));
#61338=CARTESIAN_POINT('Ctrl Pts',(66.6246270342296,-3.5004660881799,338.457555281479));
#61339=CARTESIAN_POINT('Ctrl Pts',(66.6168750607065,-3.40268599578553,338.553832846817));
#61340=CARTESIAN_POINT('Ctrl Pts',(66.6091230871835,-3.3009985301378,338.64590067974));
#61341=CARTESIAN_POINT('Ctrl Pts',(66.6013743966259,-3.19935412919243,338.737929521881));
#61342=CARTESIAN_POINT('Ctrl Pts',(66.5936257060683,-3.09380593537663,338.82575191572));
#61343=CARTESIAN_POINT('Ctrl Pts',(66.5858770155107,-2.9847419686626,338.909027813025));
#61344=CARTESIAN_POINT('Ctrl Pts',(66.5781299371328,-2.87570069361768,338.992286384084));
#61345=CARTESIAN_POINT('Ctrl Pts',(66.570382858755,-2.7631454111238,339.071000103083));
#61346=CARTESIAN_POINT('Ctrl Pts',(66.5626357803772,-2.64749667611866,339.144869649632));
#61347=CARTESIAN_POINT('Ctrl Pts',(66.5548886370714,-2.53184697186582,339.218739815279));
#61348=CARTESIAN_POINT('Ctrl Pts',(66.5471414937655,-2.41310409280062,339.287765517091));
#61349=CARTESIAN_POINT('Ctrl Pts',(66.5393943504597,-2.29171664145694,339.351691383562));
#61350=CARTESIAN_POINT('Ctrl Pts',(66.5316454654316,-2.17030189963691,339.415631621925));
#61351=CARTESIAN_POINT('Ctrl Pts',(66.5238965804035,-2.04624174821828,339.474469561341));
#61352=CARTESIAN_POINT('Ctrl Pts',(66.5161476953754,-1.92000802614176,339.527996493158));
#61353=CARTESIAN_POINT('Ctrl Pts',(66.5083905856007,-1.79364031828855,339.581580239013));
#61354=CARTESIAN_POINT('Ctrl Pts',(66.500633475826,-1.66509479165551,339.629841563685));
#61355=CARTESIAN_POINT('Ctrl Pts',(66.4928763660512,-1.53486236071531,339.672620313717));
#61356=CARTESIAN_POINT('Ctrl Pts',(66.4851151111251,-1.40456033772804,339.715421923345));
#61357=CARTESIAN_POINT('Ctrl Pts',(66.4773538561989,-1.27256999020031,339.75273501434));
#61358=CARTESIAN_POINT('Ctrl Pts',(66.4695926012727,-1.13939495128114,339.784450042324));
#61359=CARTESIAN_POINT('Ctrl Pts',(66.461818930868,-1.00600687570125,339.816215804017));
#61360=CARTESIAN_POINT('Ctrl Pts',(66.4540452604634,-0.871430705618236,
339.842365533209));
#61361=CARTESIAN_POINT('Ctrl Pts',(66.4462715900587,-0.736178650228208,
339.862841150752));
#61362=CARTESIAN_POINT('Ctrl Pts',(66.4388597858816,-0.607222610555794,
339.882363623373));
#61363=CARTESIAN_POINT('Ctrl Pts',(66.4314479817045,-0.477652480456083,
339.896728324271));
#61364=CARTESIAN_POINT('Ctrl Pts',(66.4240361775274,-0.347912518367584,
339.905929060032));
#61365=CARTESIAN_POINT('Ctrl Pts',(66.4162610987489,-0.211813614262213,
339.91558075126));
#61366=CARTESIAN_POINT('Ctrl Pts',(66.4084860199704,-0.0750977115996171,
339.919579976508));
#61367=CARTESIAN_POINT('Ctrl Pts',(66.400710941192,0.061726262174502,339.91786263849));
#61368=CARTESIAN_POINT('Ctrl Pts',(66.392945430143,0.198381865338344,339.916147413766));
#61369=CARTESIAN_POINT('Ctrl Pts',(66.385179919094,0.335144887897763,339.908729627461));
#61370=CARTESIAN_POINT('Ctrl Pts',(66.3774144080449,0.471501484549826,339.895596941392));
#61371=CARTESIAN_POINT('Ctrl Pts',(66.3696565965227,0.607722883239224,339.88247727642));
#61372=CARTESIAN_POINT('Ctrl Pts',(66.3618987850005,0.743538271391627,339.863654025252));
#61373=CARTESIAN_POINT('Ctrl Pts',(66.3541409734783,0.878434363935561,339.839166883954));
#61374=CARTESIAN_POINT('Ctrl Pts',(66.3463889999553,1.01322894289169,339.814698170007));
#61375=CARTESIAN_POINT('Ctrl Pts',(66.3386370264323,1.14710522019096,339.784574119275));
#61376=CARTESIAN_POINT('Ctrl Pts',(66.3308850529093,1.27955594756414,339.748886147251));
#61377=CARTESIAN_POINT('Ctrl Pts',(66.3231363623517,1.41195058197591,339.713213289104));
#61378=CARTESIAN_POINT('Ctrl Pts',(66.3153876717941,1.54292049059182,339.671981297707));
#61379=CARTESIAN_POINT('Ctrl Pts',(66.3076389812364,1.6719697397272,339.625332447721));
#61380=CARTESIAN_POINT('Ctrl Pts',(66.2998919028586,1.80099213908838,339.578693303417));
#61381=CARTESIAN_POINT('Ctrl Pts',(66.2921448244808,1.928094306456,339.526639675049));
#61382=CARTESIAN_POINT('Ctrl Pts',(66.2843977461029,2.05279695052103,339.469363236797));
#61383=CARTESIAN_POINT('Ctrl Pts',(66.2766506027971,2.1775006397145,339.412086318513));
#61384=CARTESIAN_POINT('Ctrl Pts',(66.2689034594913,2.2998044102945,339.349586666183));
#61385=CARTESIAN_POINT('Ctrl Pts',(66.2611563161855,2.41925075034118,339.282103323073));
#61386=CARTESIAN_POINT('Ctrl Pts',(66.2534074311574,2.53872394446045,339.214604808275));
#61387=CARTESIAN_POINT('Ctrl Pts',(66.2456585461293,2.65533808946972,339.142120565378));
#61388=CARTESIAN_POINT('Ctrl Pts',(66.2379096611012,2.76866233868613,339.064934429587));
#61389=CARTESIAN_POINT('Ctrl Pts',(66.2301525513265,2.8821068714319,338.987666367633));
#61390=CARTESIAN_POINT('Ctrl Pts',(66.2223954415518,2.99225420936034,338.905686663903));
#61391=CARTESIAN_POINT('Ctrl Pts',(66.2146383317771,3.09870401402384,338.819321470624));
#61392=CARTESIAN_POINT('Ctrl Pts',(66.2068770768509,3.20521070205928,338.732910126548));
#61393=CARTESIAN_POINT('Ctrl Pts',(66.1991158219247,3.30801562696851,338.642108881984));
#61394=CARTESIAN_POINT('Ctrl Pts',(66.1913545669986,3.40675412575205,338.547281972042));
#61395=CARTESIAN_POINT('Ctrl Pts',(66.1835808965939,3.50565057395484,338.452303369948));
#61396=CARTESIAN_POINT('Ctrl Pts',(66.1758072261892,3.60046732672272,338.353286516405));
#61397=CARTESIAN_POINT('Ctrl Pts',(66.1680335557845,3.69087835827589,338.250630709095));
#61398=CARTESIAN_POINT('Ctrl Pts',(66.1606217516075,3.77708073455789,338.152753554314));
#61399=CARTESIAN_POINT('Ctrl Pts',(66.1532099474305,3.85927815012865,338.051568831559));
#61400=CARTESIAN_POINT('Ctrl Pts',(66.1457981432535,3.9372249830816,337.947446775617));
#61401=CARTESIAN_POINT('Ctrl Pts',(66.138023064475,4.01899222250997,337.83822138755));
#61402=CARTESIAN_POINT('Ctrl Pts',(66.1302479856966,4.09634007602878,337.725418278553));
#61403=CARTESIAN_POINT('Ctrl Pts',(66.1224729069182,4.16893923301867,337.609430729852));
#61404=CARTESIAN_POINT('Ctrl Pts',(66.1147073958692,4.2414490521239,337.493585911215));
#61405=CARTESIAN_POINT('Ctrl Pts',(66.1069418848202,4.30922159633566,337.374564778032));
#61406=CARTESIAN_POINT('Ctrl Pts',(66.0991763737712,4.37196841903521,337.252792756882));
#61407=CARTESIAN_POINT('Ctrl Pts',(66.091418562249,4.43465302807729,337.131141473046));
#61408=CARTESIAN_POINT('Ctrl Pts',(66.0836607507268,4.49232165420805,337.006745074369));
#61409=CARTESIAN_POINT('Ctrl Pts',(66.0759029392046,4.54472991069206,336.88005667504));
#61410=CARTESIAN_POINT('Ctrl Pts',(66.0681509656816,4.59709872830131,336.753463612747));
#61411=CARTESIAN_POINT('Ctrl Pts',(66.0603989921586,4.64421490683903,336.624582342672));
#61412=CARTESIAN_POINT('Ctrl Pts',(66.0526470186356,4.6858808183973,336.493888890874));
#61413=CARTESIAN_POINT('Ctrl Pts',(66.0448983280779,4.72752908441718,336.36325078783));
#61414=CARTESIAN_POINT('Ctrl Pts',(66.0371496375203,4.76373155580886,336.230802401118));
#61415=CARTESIAN_POINT('Ctrl Pts',(66.0294009469627,4.79433949619766,336.097037764938));
#61416=CARTESIAN_POINT('Ctrl Pts',(66.0216538685849,4.82494106834879,335.963300959607));
#61417=CARTESIAN_POINT('Ctrl Pts',(66.013906790207,4.84995033762177,335.828248830315));
#61418=CARTESIAN_POINT('Ctrl Pts',(66.0061597118292,4.86926911489622,335.692388149247));
#61419=CARTESIAN_POINT('Ctrl Pts',(65.9984125685234,4.88858805408062,335.556526329536));
#61420=CARTESIAN_POINT('Ctrl Pts',(65.9906654252176,4.90221635111459,335.419856331514));
#61421=CARTESIAN_POINT('Ctrl Pts',(65.9829182819119,4.91010743662831,335.282892246743));
#61422=CARTESIAN_POINT('Ctrl Pts',(65.9751693968838,4.91800029622556,335.145897369538));
#61423=CARTESIAN_POINT('Ctrl Pts',(65.9674205118557,4.92015335517299,335.00860866417));
#61424=CARTESIAN_POINT('Ctrl Pts',(65.9596716268276,4.91657214068717,334.871542038321));
#61425=CARTESIAN_POINT('Ctrl Pts',(65.9519145170529,4.91298712506329,334.734329928539));
#61426=CARTESIAN_POINT('Ctrl Pts',(65.9441574072782,4.90365568804226,334.597340760501));
#61427=CARTESIAN_POINT('Ctrl Pts',(65.9364002975035,4.88863545188595,334.461087687036));
#61428=CARTESIAN_POINT('Ctrl Pts',(65.9286390425773,4.87360718939566,334.324761804285));
#61429=CARTESIAN_POINT('Ctrl Pts',(65.9208777876511,4.85288412949549,334.189173186074));
#61430=CARTESIAN_POINT('Ctrl Pts',(65.9131165327249,4.82657522518768,334.054825593816));
#61431=CARTESIAN_POINT('Ctrl Pts',(65.9053428623202,4.80022423520704,333.920263089195));
#61432=CARTESIAN_POINT('Ctrl Pts',(65.8975691919156,4.76826963613787,333.786945957928));
#61433=CARTESIAN_POINT('Ctrl Pts',(65.8897955215109,4.73087077466268,333.655364444936));
#61434=CARTESIAN_POINT('Ctrl Pts',(65.8823837173338,4.6952128391867,333.52990808303));
#61435=CARTESIAN_POINT('Ctrl Pts',(65.8749719131567,4.65460618519243,333.406029663209));
#61436=CARTESIAN_POINT('Ctrl Pts',(65.8675601089796,4.60922923090351,333.284136089463));
#61437=CARTESIAN_POINT('Ctrl Pts',(65.8597850302011,4.56162821691407,333.156268148565));
#61438=CARTESIAN_POINT('Ctrl Pts',(65.8520099514227,4.50862703776745,333.030180453478));
#61439=CARTESIAN_POINT('Ctrl Pts',(65.8442348726443,4.45037820316542,332.906362755564));
#61440=CARTESIAN_POINT('Ctrl Pts',(65.8364693615953,4.39220104746271,332.78269742321));
#61441=CARTESIAN_POINT('Ctrl Pts',(65.8287038505462,4.32878924982514,332.661296880322));
#61442=CARTESIAN_POINT('Ctrl Pts',(65.8209383394972,4.26034446552274,332.542633910548));
#61443=CARTESIAN_POINT('Ctrl Pts',(65.813180527975,4.19196754442321,332.424088595454));
#61444=CARTESIAN_POINT('Ctrl Pts',(65.8054227164528,4.11856776151994,332.308275788246));
#61445=CARTESIAN_POINT('Ctrl Pts',(65.7976649049306,4.04039389851348,332.195646205031));
#61446=CARTESIAN_POINT('Ctrl Pts',(65.7899129314077,3.96227886381819,332.08310137915));
#61447=CARTESIAN_POINT('Ctrl Pts',(65.7821609578847,3.87939712198385,331.973735328995));
#61448=CARTESIAN_POINT('Ctrl Pts',(65.7744089843617,3.79204202567799,331.867971849106));
#61449=CARTESIAN_POINT('Ctrl Pts',(65.7666602938041,3.70472392430709,331.762253160113));
#61450=CARTESIAN_POINT('Ctrl Pts',(65.7589116032464,3.61293648482616,331.660134307638));
#61451=CARTESIAN_POINT('Ctrl Pts',(65.7511629126888,3.51701466134618,331.562007717522));
#61452=CARTESIAN_POINT('Ctrl Pts',(65.743415834311,3.42111279520265,331.463901543464));
#61453=CARTESIAN_POINT('Ctrl Pts',(65.7356687559332,3.32107852910539,331.369786258933));
#61454=CARTESIAN_POINT('Ctrl Pts',(65.7279216775553,3.21728488282916,331.280018676765));
#61455=CARTESIAN_POINT('Ctrl Pts',(65.7201745342495,3.11349036666256,331.190250342258));
#61456=CARTESIAN_POINT('Ctrl Pts',(65.7124273909438,3.00593670311625,331.104830038483));
#61457=CARTESIAN_POINT('Ctrl Pts',(65.704680247638,2.89503100139379,331.024075131058));
#61458=CARTESIAN_POINT('Ctrl Pts',(65.6969313626099,2.7841003657146,330.943302068216));
#61459=CARTESIAN_POINT('Ctrl Pts',(65.6891824775817,2.66981650818277,330.867196718914));
#61460=CARTESIAN_POINT('Ctrl Pts',(65.6814335925536,2.5526162576692,330.796033622449));
#61461=CARTESIAN_POINT('Ctrl Pts',(65.6736764827789,2.43529160959892,330.724794992737));
#61462=CARTESIAN_POINT('Ctrl Pts',(65.6659193730042,2.3150447196508,330.658509297944));
#61463=CARTESIAN_POINT('Ctrl Pts',(65.6581622632294,2.19233829169693,330.597405778719));
#61464=CARTESIAN_POINT('Ctrl Pts',(65.6504010083033,2.06956629335136,330.536269607727));
#61465=CARTESIAN_POINT('Ctrl Pts',(65.6426397533771,1.9443324948402,330.480321289516));
#61466=CARTESIAN_POINT('Ctrl Pts',(65.6348784984509,1.81711948060543,330.429741817391));
#61467=CARTESIAN_POINT('Ctrl Pts',(65.6271048280462,1.68970296700651,330.379081434594));
#61468=CARTESIAN_POINT('Ctrl Pts',(65.6193311576416,1.56030128001685,330.333807189209));
#61469=CARTESIAN_POINT('Ctrl Pts',(65.6115574872369,1.42941290868267,330.294050382867));
#61470=CARTESIAN_POINT('Ctrl Pts',(65.6041456830598,1.30461742252375,330.256144265426));
#61471=CARTESIAN_POINT('Ctrl Pts',(65.5967338788827,1.17847082598085,330.223253545967));
#61472=CARTESIAN_POINT('Ctrl Pts',(65.5893220747056,1.05141184563745,330.195448387898));
#61473=CARTESIAN_POINT('Ctrl Pts',(65.5815469959272,0.918125326178437,330.166280416204));
#61474=CARTESIAN_POINT('Ctrl Pts',(65.5737719171487,0.783413514173073,330.142616951757));
#61475=CARTESIAN_POINT('Ctrl Pts',(65.5659968383703,0.647770783741957,330.124594778459));
#61476=CARTESIAN_POINT('Ctrl Pts',(65.5582313273213,0.512294970326168,330.106594782593));
#61477=CARTESIAN_POINT('Ctrl Pts',(65.5504658162723,0.375890901574579,330.094222316339));
#61478=CARTESIAN_POINT('Ctrl Pts',(65.5427003052233,0.239065278581079,330.08756365384));
#61479=CARTESIAN_POINT('Ctrl Pts',(65.5349424937011,0.102375318590763,330.080911593424));
#61480=CARTESIAN_POINT('Ctrl Pts',(65.5271846821788,-0.0347349759557258,
330.079962081465));
#61481=CARTESIAN_POINT('Ctrl Pts',(65.5194268706566,-0.171751958216401,
330.084749820472));
#61482=CARTESIAN_POINT('Ctrl Pts',(65.5116748971336,-0.308665830852681,
330.089533956553));
#61483=CARTESIAN_POINT('Ctrl Pts',(65.5039229236106,-0.445486141910531,
330.100046736305));
#61484=CARTESIAN_POINT('Ctrl Pts',(65.4961709500876,-0.581697763560121,
330.116270812753));
#61485=CARTESIAN_POINT('Ctrl Pts',(65.4884222595299,-0.717851699506703,
330.132488018295));
#61486=CARTESIAN_POINT('Ctrl Pts',(65.4806735689723,-0.853397071428923,
330.1544116637));
#61487=CARTESIAN_POINT('Ctrl Pts',(65.4729248784147,-0.987822617173819,
330.181972443053));
#61488=CARTESIAN_POINT('Ctrl Pts',(65.4651778000368,-1.12222019456155,330.209527488156));
#61489=CARTESIAN_POINT('Ctrl Pts',(65.457430721659,-1.25549802653516,330.242717255861));
#61490=CARTESIAN_POINT('Ctrl Pts',(65.4496836432811,-1.38715419916627,330.281421157781));
#61491=CARTESIAN_POINT('Ctrl Pts',(65.4419364999753,-1.51881147520283,330.320125384077));
#61492=CARTESIAN_POINT('Ctrl Pts',(65.4341893566695,-1.64884668978292,330.364343726522));
#61493=CARTESIAN_POINT('Ctrl Pts',(65.4264422133637,-1.77677265323683,330.413905583047));
#61494=CARTESIAN_POINT('Ctrl Pts',(65.4186933283356,-1.90472737716292,330.463478582129));
#61495=CARTESIAN_POINT('Ctrl Pts',(65.4109444433075,-2.03057154194372,330.518397344636));
#61496=CARTESIAN_POINT('Ctrl Pts',(65.4031955582794,-2.15383788846126,330.578443100815));
#61497=CARTESIAN_POINT('Ctrl Pts',(65.3954384485047,-2.27723507115273,330.638552590181));
#61498=CARTESIAN_POINT('Ctrl Pts',(65.38768133873,-2.39804861796368,330.703799772368));
#61499=CARTESIAN_POINT('Ctrl Pts',(65.3799242289552,-2.51583535992565,330.773919605089));
#61500=CARTESIAN_POINT('Ctrl Pts',(65.3721629740291,-2.63368504335643,330.844076907607));
#61501=CARTESIAN_POINT('Ctrl Pts',(65.3644017191029,-2.74850437203266,330.919111835224));
#61502=CARTESIAN_POINT('Ctrl Pts',(65.3566404641767,-2.85987999069209,330.998716518248));
#61503=CARTESIAN_POINT('Ctrl Pts',(65.3488667937721,-2.97143377404422,331.078448542822));
#61504=CARTESIAN_POINT('Ctrl Pts',(65.3410931233674,-3.07953253076973,331.162764690062));
#61505=CARTESIAN_POINT('Ctrl Pts',(65.3333194529628,-3.18379608549871,331.251316824742));
#61506=CARTESIAN_POINT('Ctrl Pts',(65.3259076487857,-3.28320614666963,331.335746836247));
#61507=CARTESIAN_POINT('Ctrl Pts',(65.3184958446087,-3.37912981603328,331.42402714493));
#61508=CARTESIAN_POINT('Ctrl Pts',(65.3110840404317,-3.47127067155644,331.515826785693));
#61509=CARTESIAN_POINT('Ctrl Pts',(65.3034172238383,-3.56658174874906,331.610784908204));
#61510=CARTESIAN_POINT('Ctrl Pts',(65.295750407245,-3.65816456085217,331.709827552767));
#61511=CARTESIAN_POINT('Ctrl Pts',(65.2880835906516,-3.7456412172627,331.812625699099));
#61512=CARTESIAN_POINT('Ctrl Pts',(65.2804263833121,-3.83300823424355,331.915295002714));
#61513=CARTESIAN_POINT('Ctrl Pts',(65.2727691759726,-3.91627907234102,332.021710143298));
#61514=CARTESIAN_POINT('Ctrl Pts',(65.2651119686331,-3.99511118947942,332.131503940007));
#61515=CARTESIAN_POINT('Ctrl Pts',(65.2574635671177,-4.07385264931564,332.241171473337));
#61516=CARTESIAN_POINT('Ctrl Pts',(65.2498151656024,-4.14816531583106,332.354209603464));
#61517=CARTESIAN_POINT('Ctrl Pts',(65.242166764087,-4.2177460886557,332.47021720416));
#61518=CARTESIAN_POINT('Ctrl Pts',(65.2345232922065,-4.28728201448842,332.586150034316));
#61519=CARTESIAN_POINT('Ctrl Pts',(65.2268798203259,-4.35209190408787,332.705048185819));
#61520=CARTESIAN_POINT('Ctrl Pts',(65.2192363484454,-4.41191535082616,332.826480734007));
#61521=CARTESIAN_POINT('Ctrl Pts',(65.2115960398435,-4.47171403941285,332.947863026891));
#61522=CARTESIAN_POINT('Ctrl Pts',(65.2039557312417,-4.5265302118481,333.071777269771));
#61523=CARTESIAN_POINT('Ctrl Pts',(65.1963154226399,-4.57614917568522,333.197767555398));
#61524=CARTESIAN_POINT('Ctrl Pts',(65.1886765138843,-4.62575904840789,333.323734757268));
#61525=CARTESIAN_POINT('Ctrl Pts',(65.1810376051287,-4.67017346056786,333.451776870211));
#61526=CARTESIAN_POINT('Ctrl Pts',(65.1733986963731,-4.7092258960529,333.581418129805));
#61527=CARTESIAN_POINT('Ctrl Pts',(65.1657567665039,-4.7482937763937,333.711110661248));
#61528=CARTESIAN_POINT('Ctrl Pts',(65.1581148366347,-4.78199532455701,333.842403217695));
#61529=CARTESIAN_POINT('Ctrl Pts',(65.1504729067655,-4.81021396004182,333.974805032631));
#61530=CARTESIAN_POINT('Ctrl Pts',(65.1428293646065,-4.83843854907786,334.107234781624));
#61531=CARTESIAN_POINT('Ctrl Pts',(65.1351858224473,-4.8611778491727,334.240773858928));
#61532=CARTESIAN_POINT('Ctrl Pts',(65.1275422802883,-4.87836666943963,334.374922643987));
#61533=CARTESIAN_POINT('Ctrl Pts',(65.1198917627945,-4.89557117585986,334.509193850386));
#61534=CARTESIAN_POINT('Ctrl Pts',(65.1122412453008,-4.90721504923341,334.64407547474));
#61535=CARTESIAN_POINT('Ctrl Pts',(65.104590727807,-4.91328508657738,334.779063989996));
#61536=CARTESIAN_POINT('Ctrl Pts',(65.1003329440526,-4.91666327719168,334.854189876286));
#61537=CARTESIAN_POINT('Ctrl Pts',(65.0960751602982,-4.9183160066904,334.929348859592));
#61538=CARTESIAN_POINT('Ctrl Pts',(65.0918173765437,-4.91824798275492,335.004454506388));
#61539=CARTESIAN_POINT('',(63.341817376473,-4.91824948425114,334.997747631595));
#61540=CARTESIAN_POINT('Ctrl Pts',(65.0918173765086,-4.91824798275436,335.004454507007));
#61541=CARTESIAN_POINT('Ctrl Pts',(65.0809789349072,-4.91807482375963,335.195640394707));
#61542=CARTESIAN_POINT('Ctrl Pts',(65.0701404933059,-4.90675037086299,335.386341402681));
#61543=CARTESIAN_POINT('Ctrl Pts',(65.0593020517045,-4.88446398368072,335.575495138664));
#61544=CARTESIAN_POINT('Ctrl Pts',(65.0504833698556,-4.86633069797861,335.72939979392));
#61545=CARTESIAN_POINT('Ctrl Pts',(65.0416646880067,-4.84094124615037,335.882281032344));
#61546=CARTESIAN_POINT('Ctrl Pts',(65.0328460061578,-4.80841932933467,336.033579515945));
#61547=CARTESIAN_POINT('Ctrl Pts',(65.0250709273793,-4.77974605711561,336.166973332527));
#61548=CARTESIAN_POINT('Ctrl Pts',(65.0172958486009,-4.74547240905112,336.299383864177));
#61549=CARTESIAN_POINT('Ctrl Pts',(65.0095207698225,-4.70567871032785,336.430304491242));
#61550=CARTESIAN_POINT('Ctrl Pts',(65.0017552587735,-4.66593398028416,336.561064012141));
#61551=CARTESIAN_POINT('Ctrl Pts',(64.9939897477244,-4.62068282783947,336.690336906035));
#61552=CARTESIAN_POINT('Ctrl Pts',(64.9862242366754,-4.57005665624649,336.817626260043));
#61553=CARTESIAN_POINT('Ctrl Pts',(64.9784664251532,-4.51948068065022,336.944789406285));
#61554=CARTESIAN_POINT('Ctrl Pts',(64.970708613631,-4.46354043513179,337.069972565595));
#61555=CARTESIAN_POINT('Ctrl Pts',(64.9629508021088,-4.40241713803768,337.19269386947));
#61556=CARTESIAN_POINT('Ctrl Pts',(64.9551988285858,-4.34133983816296,337.315322821673));
#61557=CARTESIAN_POINT('Ctrl Pts',(64.9474468550628,-4.27508742385039,337.435493257528));
#61558=CARTESIAN_POINT('Ctrl Pts',(64.9396948815398,-4.20388909941276,337.55274352459));
#61559=CARTESIAN_POINT('Ctrl Pts',(64.9319461909822,-4.13272092750776,337.669944136095));
#61560=CARTESIAN_POINT('Ctrl Pts',(64.9241975004246,-4.05661121393649,337.784226705096));
#61561=CARTESIAN_POINT('Ctrl Pts',(64.916448809867,-3.97583485146533,337.895154623915));
#61562=CARTESIAN_POINT('Ctrl Pts',(64.9087017314891,-3.89507529519104,338.006059463253));
#61563=CARTESIAN_POINT('Ctrl Pts',(64.9009546531113,-3.80965125122163,338.113610724927));
#61564=CARTESIAN_POINT('Ctrl Pts',(64.8932075747335,-3.71988041368792,338.21740155566));
#61565=CARTESIAN_POINT('Ctrl Pts',(64.8854604314277,-3.63010882378819,338.321193256259));
#61566=CARTESIAN_POINT('Ctrl Pts',(64.8777132881219,-3.53599062336178,338.421224167421));
#61567=CARTESIAN_POINT('Ctrl Pts',(64.869966144816,-3.4378829258465,338.517121557563));
#61568=CARTESIAN_POINT('Ctrl Pts',(64.862217259788,-3.33975317163807,338.613040507474));
#61569=CARTESIAN_POINT('Ctrl Pts',(64.8544683747599,-3.23763241502894,338.704823813985));
#61570=CARTESIAN_POINT('Ctrl Pts',(64.8467194897318,-3.13191335169259,338.792136840884));
#61571=CARTESIAN_POINT('Ctrl Pts',(64.8389623799571,-3.02608207704992,338.879542542732));
#61572=CARTESIAN_POINT('Ctrl Pts',(64.8312052701824,-2.91664516816334,338.962468237482));
#61573=CARTESIAN_POINT('Ctrl Pts',(64.8234481604076,-2.80402745477987,339.040620384958));
#61574=CARTESIAN_POINT('Ctrl Pts',(64.8156869054815,-2.69134956209119,339.118814294444));
#61575=CARTESIAN_POINT('Ctrl Pts',(64.8079256505552,-2.57548780806422,339.19222936479));
#61576=CARTESIAN_POINT('Ctrl Pts',(64.8001643956291,-2.45689364970565,339.260616933794));
#61577=CARTESIAN_POINT('Ctrl Pts',(64.7923907252244,-2.33810977934354,339.329113900622));
#61578=CARTESIAN_POINT('Ctrl Pts',(64.7846170548198,-2.21658511685253,339.392567114074));
#61579=CARTESIAN_POINT('Ctrl Pts',(64.7768433844151,-2.09279402023467,339.450774792255));
#61580=CARTESIAN_POINT('Ctrl Pts',(64.769431580238,-1.97476542894603,339.506272889012));
#61581=CARTESIAN_POINT('Ctrl Pts',(64.7620197760609,-1.85467692512314,339.557002707616));
#61582=CARTESIAN_POINT('Ctrl Pts',(64.7546079718837,-1.73295254073325,339.602831580024));
#61583=CARTESIAN_POINT('Ctrl Pts',(64.7468328931053,-1.605262081667,339.650906661986));
#61584=CARTESIAN_POINT('Ctrl Pts',(64.7390578143269,-1.47536780315882,339.693740156522));
#61585=CARTESIAN_POINT('Ctrl Pts',(64.7312827355484,-1.3437392010497,339.731125449833));
#61586=CARTESIAN_POINT('Ctrl Pts',(64.7235172244994,-1.21227257631528,339.768464738161));
#61587=CARTESIAN_POINT('Ctrl Pts',(64.7157517134504,-1.0790762468255,339.800369059242));
#61588=CARTESIAN_POINT('Ctrl Pts',(64.7079862024014,-0.944639187063109,
339.826680004803));
#61589=CARTESIAN_POINT('Ctrl Pts',(64.7002283908792,-0.810335422036691,
339.852964862984));
#61590=CARTESIAN_POINT('Ctrl Pts',(64.692470579357,-0.674793756006488,339.873667307606));
#61591=CARTESIAN_POINT('Ctrl Pts',(64.6847127678348,-0.538517470121591,
339.888678962345));
#61592=CARTESIAN_POINT('Ctrl Pts',(64.6769607943118,-0.402343736463855,
339.903679320338));
#61593=CARTESIAN_POINT('Ctrl Pts',(64.6692088207887,-0.265436870281805,
339.912997369928));
#61594=CARTESIAN_POINT('Ctrl Pts',(64.6614568472657,-0.128309120572251,
339.916576027285));
#61595=CARTESIAN_POINT('Ctrl Pts',(64.6537081567081,0.00876055545407584,
339.920153169079));
#61596=CARTESIAN_POINT('Ctrl Pts',(64.6459594661505,0.146050539026823,339.917995742826));
#61597=CARTESIAN_POINT('Ctrl Pts',(64.6382107755929,0.283044917184179,339.910098638251));
#61598=CARTESIAN_POINT('Ctrl Pts',(64.6304636972151,0.42001079251696,339.902203176735));
#61599=CARTESIAN_POINT('Ctrl Pts',(64.6227166188372,0.556680794787046,339.888570434701));
#61600=CARTESIAN_POINT('Ctrl Pts',(64.6149695404594,0.692540869869353,339.869247396268));
#61601=CARTESIAN_POINT('Ctrl Pts',(64.6072223971536,0.828402083589853,339.849924195889));
#61602=CARTESIAN_POINT('Ctrl Pts',(64.5994752538478,0.963452969603614,339.824910659029));
#61603=CARTESIAN_POINT('Ctrl Pts',(64.591728110542,1.097186835399,339.794305383549));
#61604=CARTESIAN_POINT('Ctrl Pts',(64.5839792255139,1.23095076740658,339.763693227354));
#61605=CARTESIAN_POINT('Ctrl Pts',(64.5762303404858,1.36339670905216,339.727486918148));
#61606=CARTESIAN_POINT('Ctrl Pts',(64.5684814554577,1.49403074744294,339.685835591247));
#61607=CARTESIAN_POINT('Ctrl Pts',(64.5607243456829,1.62480344215194,339.644140055196));
#61608=CARTESIAN_POINT('Ctrl Pts',(64.5529672359082,1.75376001889645,339.596988075484));
#61609=CARTESIAN_POINT('Ctrl Pts',(64.5452101261335,1.88042373372718,339.544578049075));
#61610=CARTESIAN_POINT('Ctrl Pts',(64.5374488712073,2.00715513359711,339.492140016424));
#61611=CARTESIAN_POINT('Ctrl Pts',(64.5296876162812,2.13159087574279,339.43443850278));
#61612=CARTESIAN_POINT('Ctrl Pts',(64.521926361355,2.2532775455229,339.371718582588));
#61613=CARTESIAN_POINT('Ctrl Pts',(64.5141526909504,2.37515887431708,339.308898330963));
#61614=CARTESIAN_POINT('Ctrl Pts',(64.5063790205457,2.49428200318152,339.241043824403));
#61615=CARTESIAN_POINT('Ctrl Pts',(64.498605350141,2.61022054708114,339.168444764909));
#61616=CARTESIAN_POINT('Ctrl Pts',(64.491193545964,2.72076212386839,339.099225209101));
#61617=CARTESIAN_POINT('Ctrl Pts',(64.4837817417869,2.82840869069962,339.025693039984));
#61618=CARTESIAN_POINT('Ctrl Pts',(64.4763699376099,2.93281921615969,338.948133040796));
#61619=CARTESIAN_POINT('Ctrl Pts',(64.4685948588315,3.04234721249602,338.866771595008));
#61620=CARTESIAN_POINT('Ctrl Pts',(64.460819780053,3.14866005929728,338.780720386717));
#61621=CARTESIAN_POINT('Ctrl Pts',(64.4530447012746,3.25132993947161,338.690262414408));
#61622=CARTESIAN_POINT('Ctrl Pts',(64.4452791902256,3.35387347782218,338.599915756394));
#61623=CARTESIAN_POINT('Ctrl Pts',(64.4375136791766,3.45278267875889,338.505173380113));
#61624=CARTESIAN_POINT('Ctrl Pts',(64.4297481681276,3.54765972123455,338.406360750835));
#61625=CARTESIAN_POINT('Ctrl Pts',(64.4219903566054,3.6424426928463,338.307646094566));
#61626=CARTESIAN_POINT('Ctrl Pts',(64.4142325450832,3.73320119306368,338.204869496638));
#61627=CARTESIAN_POINT('Ctrl Pts',(64.406474733561,3.81957173161708,338.098395528258));
#61628=CARTESIAN_POINT('Ctrl Pts',(64.398722760038,3.90587727360119,337.992001684917));
#61629=CARTESIAN_POINT('Ctrl Pts',(64.3909707865151,3.98780118129954,337.881916311667));
#61630=CARTESIAN_POINT('Ctrl Pts',(64.3832188129921,4.06501824437489,337.768539278284));
#61631=CARTESIAN_POINT('Ctrl Pts',(64.3754701224344,4.14220260597819,337.655210260141));
#61632=CARTESIAN_POINT('Ctrl Pts',(64.3677214318768,4.21468386802446,337.538592676863));
#61633=CARTESIAN_POINT('Ctrl Pts',(64.3599727413192,4.28217854306664,337.419117605202));
#61634=CARTESIAN_POINT('Ctrl Pts',(64.3522256629414,4.34965917527796,337.299667391328));
#61635=CARTESIAN_POINT('Ctrl Pts',(64.3444785845635,4.41215509201134,337.177361211732));
#61636=CARTESIAN_POINT('Ctrl Pts',(64.3367315061857,4.46942761903059,337.052656771296));
#61637=CARTESIAN_POINT('Ctrl Pts',(64.3289843628799,4.52670062604878,336.927951285717));
#61638=CARTESIAN_POINT('Ctrl Pts',(64.3212372195741,4.57874999290288,336.800847854412));
#61639=CARTESIAN_POINT('Ctrl Pts',(64.3134900762683,4.62538443224659,336.671825922885));
#61640=CARTESIAN_POINT('Ctrl Pts',(64.3057411912402,4.67202935600233,336.542774984489));
#61641=CARTESIAN_POINT('Ctrl Pts',(64.2979923062121,4.71325679693508,336.411805055121));
#61642=CARTESIAN_POINT('Ctrl Pts',(64.290243421184,4.74892488150428,336.279412182344));
#61643=CARTESIAN_POINT('Ctrl Pts',(64.2824863114093,4.78463082454697,336.146878786404));
#61644=CARTESIAN_POINT('Ctrl Pts',(64.2747292016346,4.81476552206692,336.012919808049));
#61645=CARTESIAN_POINT('Ctrl Pts',(64.2669720918599,4.83923781679814,335.87804351542));
#61646=CARTESIAN_POINT('Ctrl Pts',(64.2592108369337,4.86372318874118,335.743095149212));
#61647=CARTESIAN_POINT('Ctrl Pts',(64.2514495820075,4.88254007510712,335.607228878977));
#61648=CARTESIAN_POINT('Ctrl Pts',(64.2436883270814,4.89564919554401,335.470958614604));
#61649=CARTESIAN_POINT('Ctrl Pts',(64.2359146566767,4.90877928630135,335.334470362217));
#61650=CARTESIAN_POINT('Ctrl Pts',(64.2281409862721,4.9161833444349,335.197577214784));
#61651=CARTESIAN_POINT('Ctrl Pts',(64.2203673158674,4.91787424512977,335.060794502953));
#61652=CARTESIAN_POINT('Ctrl Pts',(64.2129555116903,4.91948643399049,334.930379059265));
#61653=CARTESIAN_POINT('Ctrl Pts',(64.2055437075131,4.9159053983112,334.800064288692));
#61654=CARTESIAN_POINT('Ctrl Pts',(64.198131903336,4.90718606672495,334.670291084378));
#61655=CARTESIAN_POINT('Ctrl Pts',(64.1903568245576,4.89803937472416,334.534157308747));
#61656=CARTESIAN_POINT('Ctrl Pts',(64.1825817457791,4.88320905948407,334.398189321363));
#61657=CARTESIAN_POINT('Ctrl Pts',(64.1748066670007,4.86270158409264,334.262900029465));
#61658=CARTESIAN_POINT('Ctrl Pts',(64.1670411559517,4.84221934445524,334.127777219654));
#61659=CARTESIAN_POINT('Ctrl Pts',(64.1592756449027,4.81607390303674,333.993331826329));
#61660=CARTESIAN_POINT('Ctrl Pts',(64.1515101338537,4.78432366672865,333.860074513628));
#61661=CARTESIAN_POINT('Ctrl Pts',(64.1437523223315,4.75260491087231,333.726949325941));
#61662=CARTESIAN_POINT('Ctrl Pts',(64.1359945108093,4.71529250922094,333.595010252401));
#61663=CARTESIAN_POINT('Ctrl Pts',(64.1282366992871,4.67249633203974,333.464760250132));
#61664=CARTESIAN_POINT('Ctrl Pts',(64.1204847257641,4.62973236033901,333.33460826512));
#61665=CARTESIAN_POINT('Ctrl Pts',(64.1127327522411,4.58149294865365,333.206143191203));
#61666=CARTESIAN_POINT('Ctrl Pts',(64.104980778718,4.52793836603238,333.079854897173));
#61667=CARTESIAN_POINT('Ctrl Pts',(64.0972320881604,4.47440646380866,332.953620086309));
#61668=CARTESIAN_POINT('Ctrl Pts',(64.0894833976028,4.41556401997028,332.829560580907));
#61669=CARTESIAN_POINT('Ctrl Pts',(64.0817347070451,4.35162012483087,332.708148051975));
#61670=CARTESIAN_POINT('Ctrl Pts',(64.0739876286673,4.2876895337529,332.586760783933));
#61671=CARTESIAN_POINT('Ctrl Pts',(64.0662405502894,4.21865978460155,332.468019742553));
#61672=CARTESIAN_POINT('Ctrl Pts',(64.0584934719116,4.14478661085327,332.352373324467));
#61673=CARTESIAN_POINT('Ctrl Pts',(64.0507463286058,4.07091281797669,332.236725937154));
#61674=CARTESIAN_POINT('Ctrl Pts',(64.0429991853,3.99219572995644,332.124173554269));
#61675=CARTESIAN_POINT('Ctrl Pts',(64.0352520419942,3.90893500618586,332.015136488897));
#61676=CARTESIAN_POINT('Ctrl Pts',(64.0275031569661,3.82565556363695,331.906074909678));
#61677=CARTESIAN_POINT('Ctrl Pts',(64.019754271938,3.73783068982879,331.800530531214));
#61678=CARTESIAN_POINT('Ctrl Pts',(64.0120053869099,3.64580074582721,331.698891097794));
#61679=CARTESIAN_POINT('Ctrl Pts',(64.0042482771352,3.55367312029216,331.597143783228));
#61680=CARTESIAN_POINT('Ctrl Pts',(63.9964911673604,3.45733177146089,331.499309983436));
#61681=CARTESIAN_POINT('Ctrl Pts',(63.9887340575857,3.35715478242821,331.405741407561));
#61682=CARTESIAN_POINT('Ctrl Pts',(63.9809728026595,3.25692426201564,331.312122831631));
#61683=CARTESIAN_POINT('Ctrl Pts',(63.9732115477333,3.15285431372051,331.222774275616));
#61684=CARTESIAN_POINT('Ctrl Pts',(63.9654502928072,3.04535583847942,331.138006877331));
#61685=CARTESIAN_POINT('Ctrl Pts',(63.9576766224025,2.93768540071161,331.053103878835));
#61686=CARTESIAN_POINT('Ctrl Pts',(63.9499029519979,2.82657579324869,330.972796911389));
#61687=CARTESIAN_POINT('Ctrl Pts',(63.9421292815932,2.71246733612865,330.897354022958));
#61688=CARTESIAN_POINT('Ctrl Pts',(63.9347174774161,2.60367065514083,330.825423019136));
#61689=CARTESIAN_POINT('Ctrl Pts',(63.9273056732391,2.49214828053765,330.75791358862));
#61690=CARTESIAN_POINT('Ctrl Pts',(63.919893869062,2.3783006938045,330.695018133331));
#61691=CARTESIAN_POINT('Ctrl Pts',(63.9121187902836,2.25887309771076,330.629039984422));
#61692=CARTESIAN_POINT('Ctrl Pts',(63.9043437115051,2.13650918183008,330.567931033083));
#61693=CARTESIAN_POINT('Ctrl Pts',(63.8965686327267,2.01164375834977,330.511963407904));
#61694=CARTESIAN_POINT('Ctrl Pts',(63.8888031216777,1.88693198972237,330.45606465445));
#61695=CARTESIAN_POINT('Ctrl Pts',(63.8810376106287,1.75972519163242,330.405294797125));
#61696=CARTESIAN_POINT('Ctrl Pts',(63.8732720995797,1.6304843997679,330.359881069993));
#61697=CARTESIAN_POINT('Ctrl Pts',(63.8655142880575,1.5013717505247,330.314512370703));
#61698=CARTESIAN_POINT('Ctrl Pts',(63.8577564765353,1.37022948726986,330.274489361922));
#61699=CARTESIAN_POINT('Ctrl Pts',(63.8499986650131,1.23754001448266,330.239991830358));
#61700=CARTESIAN_POINT('Ctrl Pts',(63.8422466914901,1.10495039473156,330.205520259281));
#61701=CARTESIAN_POINT('Ctrl Pts',(63.834494717967,0.970816259753514,330.17656598689));
#61702=CARTESIAN_POINT('Ctrl Pts',(63.826742744444,0.835636281442749,330.153259335632));
#61703=CARTESIAN_POINT('Ctrl Pts',(63.8189940538864,0.700513551933149,330.129962554755));
#61704=CARTESIAN_POINT('Ctrl Pts',(63.8112453633288,0.564346244407593,330.112308704221));
#61705=CARTESIAN_POINT('Ctrl Pts',(63.8034966727712,0.427644147845715,330.100377203772));
#61706=CARTESIAN_POINT('Ctrl Pts',(63.7957495943933,0.290970493296784,330.088448185772));
#61707=CARTESIAN_POINT('Ctrl Pts',(63.7880025160155,0.153762660179541,330.082239183668));
#61708=CARTESIAN_POINT('Ctrl Pts',(63.7802554376377,0.0165361068463397,
330.081777798872));
#61709=CARTESIAN_POINT('Ctrl Pts',(63.7725082943319,-0.120691596577458,
330.081316410209));
#61710=CARTESIAN_POINT('Ctrl Pts',(63.7647611510261,-0.257937629658066,
330.086602736247));
#61711=CARTESIAN_POINT('Ctrl Pts',(63.7570140077203,-0.394686379264815,
330.097612242537));
#61712=CARTESIAN_POINT('Ctrl Pts',(63.7492651226922,-0.531465872893734,
330.108624223998));
#61713=CARTESIAN_POINT('Ctrl Pts',(63.7415162376641,-0.667747471042004,
330.125361914723));
#61714=CARTESIAN_POINT('Ctrl Pts',(63.733767352636,-0.803020922363803,330.147748928513));
#61715=CARTESIAN_POINT('Ctrl Pts',(63.7260102428612,-0.938437954324471,
330.170159704111));
#61716=CARTESIAN_POINT('Ctrl Pts',(63.7182531330866,-1.07284431568034,330.198231716926));
#61717=CARTESIAN_POINT('Ctrl Pts',(63.7104960233118,-1.20573964425143,330.231837358816));
#61718=CARTESIAN_POINT('Ctrl Pts',(63.7027347683857,-1.33870598783684,330.265460958487));
#61719=CARTESIAN_POINT('Ctrl Pts',(63.6949735134595,-1.4701593153123,330.304623967764));
#61720=CARTESIAN_POINT('Ctrl Pts',(63.6872122585333,-1.59961562217729,330.34914922581));
#61721=CARTESIAN_POINT('Ctrl Pts',(63.6794385881287,-1.72927901694363,330.393745709757));
#61722=CARTESIAN_POINT('Ctrl Pts',(63.671664917724,-1.85693864320926,330.443721440994));
#61723=CARTESIAN_POINT('Ctrl Pts',(63.6638912473194,-1.98213081128307,330.498851201142));
#61724=CARTESIAN_POINT('Ctrl Pts',(63.6564794431423,-2.10149525381397,330.551414657691));
#61725=CARTESIAN_POINT('Ctrl Pts',(63.6490676389651,-2.21861653023601,330.608662975179));
#61726=CARTESIAN_POINT('Ctrl Pts',(63.641655834788,-2.33311612215949,330.670363499898));
#61727=CARTESIAN_POINT('Ctrl Pts',(63.6338807560096,-2.45322768015955,330.735088151129));
#61728=CARTESIAN_POINT('Ctrl Pts',(63.6261056772312,-2.57083363716574,330.804917018512));
#61729=CARTESIAN_POINT('Ctrl Pts',(63.6183305984527,-2.68546985261784,330.879631723598));
#61730=CARTESIAN_POINT('Ctrl Pts',(63.6105650874037,-2.79996500090858,330.954254487482));
#61731=CARTESIAN_POINT('Ctrl Pts',(63.6027995763547,-2.9114973546321,331.033750914861));
#61732=CARTESIAN_POINT('Ctrl Pts',(63.5950340653057,-3.01962633494997,331.117856280381));
#61733=CARTESIAN_POINT('Ctrl Pts',(63.5872762537835,-3.12764810506897,331.201878255186));
#61734=CARTESIAN_POINT('Ctrl Pts',(63.5795184422613,-3.23227291059481,331.290499835583));
#61735=CARTESIAN_POINT('Ctrl Pts',(63.5717606307391,-3.33308850830447,331.383412650259));
#61736=CARTESIAN_POINT('Ctrl Pts',(63.5640086572161,-3.43382823907994,331.476255545095));
#61737=CARTESIAN_POINT('Ctrl Pts',(63.5562566836931,-3.53076418149791,331.573382982637));
#61738=CARTESIAN_POINT('Ctrl Pts',(63.5485047101701,-3.6235168846556,331.674446144006));
#61739=CARTESIAN_POINT('Ctrl Pts',(63.5407560196125,-3.71623030698837,331.775466505066));
#61740=CARTESIAN_POINT('Ctrl Pts',(63.5330073290549,-3.80476374991112,331.880418987465));
#61741=CARTESIAN_POINT('Ctrl Pts',(63.5252586384972,-3.88877455160031,331.988917877353));
#61742=CARTESIAN_POINT('Ctrl Pts',(63.5175115601194,-3.97276787414055,332.09739419314));
#61743=CARTESIAN_POINT('Ctrl Pts',(63.5097644817416,-4.05224018795635,332.209415139899));
#61744=CARTESIAN_POINT('Ctrl Pts',(63.5020174033638,-4.12688933834126,332.324562194409));
#61745=CARTESIAN_POINT('Ctrl Pts',(63.494270260058,-4.20153911435796,332.439710213963));
#61746=CARTESIAN_POINT('Ctrl Pts',(63.4865231167522,-4.27136543368911,332.557984065545));
#61747=CARTESIAN_POINT('Ctrl Pts',(63.4787759734464,-4.33610990002626,332.678936882074));
#61748=CARTESIAN_POINT('Ctrl Pts',(63.4710270884183,-4.40086892229406,332.799916891365));
#61749=CARTESIAN_POINT('Ctrl Pts',(63.4632782033902,-4.46054363367496,332.923576719549));
#61750=CARTESIAN_POINT('Ctrl Pts',(63.4555293183621,-4.51492214267191,333.049445948426));
#61751=CARTESIAN_POINT('Ctrl Pts',(63.4477722085874,-4.56935836958011,333.175448776204));
#61752=CARTESIAN_POINT('Ctrl Pts',(63.4400150988127,-4.61848700947907,333.303665329808));
#61753=CARTESIAN_POINT('Ctrl Pts',(63.432257989038,-4.66214459609082,333.433605787919));
#61754=CARTESIAN_POINT('Ctrl Pts',(63.4244967341118,-4.70582551192089,333.563615682056));
#61755=CARTESIAN_POINT('Ctrl Pts',(63.4167354791856,-4.74402944020056,333.695350941057));
#61756=CARTESIAN_POINT('Ctrl Pts',(63.4089742242594,-4.77664343665158,333.828308683316));
#61757=CARTESIAN_POINT('Ctrl Pts',(63.4012005538548,-4.80930960486808,333.961479114632));
#61758=CARTESIAN_POINT('Ctrl Pts',(63.3934268834501,-4.83636789516558,334.095875553636));
#61759=CARTESIAN_POINT('Ctrl Pts',(63.3856532130455,-4.85775676938531,334.230986195188));
#61760=CARTESIAN_POINT('Ctrl Pts',(63.3782414088684,-4.87814998636424,334.35980740387));
#61761=CARTESIAN_POINT('Ctrl Pts',(63.3708296046913,-4.89338969793911,334.489277533386));
#61762=CARTESIAN_POINT('Ctrl Pts',(63.3634178005142,-4.90346670955524,334.618952377276));
#61763=CARTESIAN_POINT('Ctrl Pts',(63.356217659179,-4.91325594658029,334.744924027542));
#61764=CARTESIAN_POINT('Ctrl Pts',(63.3490175178438,-4.91819156589539,334.871277715051));
#61765=CARTESIAN_POINT('Ctrl Pts',(63.3418173765086,-4.91824948425085,334.99774763097));
#61766=CARTESIAN_POINT('',(61.5918173765632,-4.91824892677099,334.996750874583));
#61767=CARTESIAN_POINT('Ctrl Pts',(63.341817376473,-4.91824948425114,334.997747631595));
#61768=CARTESIAN_POINT('Ctrl Pts',(63.3341280999864,-4.91831133722102,335.132809167956));
#61769=CARTESIAN_POINT('Ctrl Pts',(63.3264388234998,-4.91280554215197,335.268097297782));
#61770=CARTESIAN_POINT('Ctrl Pts',(63.3187495470132,-4.90170239144568,335.403108829221));
#61771=CARTESIAN_POINT('Ctrl Pts',(63.3110692067358,-4.89061214443433,335.537963454961));
#61772=CARTESIAN_POINT('Ctrl Pts',(63.3033888664584,-4.87393751253565,335.672541726678));
#61773=CARTESIAN_POINT('Ctrl Pts',(63.2957085261811,-4.85170077901492,335.806339018903));
#61774=CARTESIAN_POINT('Ctrl Pts',(63.2880351786687,-4.8294842915049,335.940014491915));
#61775=CARTESIAN_POINT('Ctrl Pts',(63.2803618311564,-4.80171584198153,336.072910007686));
#61776=CARTESIAN_POINT('Ctrl Pts',(63.272688483644,-4.76846959825874,336.204525115131));
#61777=CARTESIAN_POINT('Ctrl Pts',(63.2648756204188,-4.73461887606246,336.338533229735));
#61778=CARTESIAN_POINT('Ctrl Pts',(63.2570627571937,-4.69508925483987,336.471213502174));
#61779=CARTESIAN_POINT('Ctrl Pts',(63.2492498939685,-4.65001379314808,336.602047061117));
#61780=CARTESIAN_POINT('Ctrl Pts',(63.2415838477446,-4.60578537612114,336.730422034746));
#61781=CARTESIAN_POINT('Ctrl Pts',(63.2339178015206,-4.55621786312987,336.857018699575));
#61782=CARTESIAN_POINT('Ctrl Pts',(63.2262517552966,-4.50148740739158,336.981361699336));
#61783=CARTESIAN_POINT('Ctrl Pts',(63.2185864449777,-4.44676220552495,337.105692762742));
#61784=CARTESIAN_POINT('Ctrl Pts',(63.2109211346588,-4.38687520759319,337.227770225173));
#61785=CARTESIAN_POINT('Ctrl Pts',(63.2032558243399,-4.32205049997778,337.347139224277));
#61786=CARTESIAN_POINT('Ctrl Pts',(63.1955895046714,-4.25721725640083,337.466523941604));
#61787=CARTESIAN_POINT('Ctrl Pts',(63.187923185003,-4.18744520120901,337.583199134887));
#61788=CARTESIAN_POINT('Ctrl Pts',(63.1802568653345,-4.11300385274006,337.696735502389));
#61789=CARTESIAN_POINT('Ctrl Pts',(63.1723337737433,-4.0360692025302,337.814074600881));
#61790=CARTESIAN_POINT('Ctrl Pts',(63.1644106821521,-3.95414725526153,337.928060547587));
#61791=CARTESIAN_POINT('Ctrl Pts',(63.1564875905609,-3.8675826693192,338.038253998349));
#61792=CARTESIAN_POINT('Ctrl Pts',(63.1488099080652,-3.78369932673884,338.145034327506));
#61793=CARTESIAN_POINT('Ctrl Pts',(63.1411322255695,-3.69545699440657,338.248253350771));
#61794=CARTESIAN_POINT('Ctrl Pts',(63.1334545430737,-3.60320816603082,338.347547456684));
#61795=CARTESIAN_POINT('Ctrl Pts',(63.1254087469348,-3.50653638159864,338.45160231105));
#61796=CARTESIAN_POINT('Ctrl Pts',(63.1173629507959,-3.40546476805529,338.551346208977));
#61797=CARTESIAN_POINT('Ctrl Pts',(63.1093171546569,-3.30043869652034,338.646407474901));
#61798=CARTESIAN_POINT('Ctrl Pts',(63.101271358518,-3.19541262498533,338.741468740824));
#61799=CARTESIAN_POINT('Ctrl Pts',(63.0932255623791,-3.08643252695116,338.83184711668));
#61800=CARTESIAN_POINT('Ctrl Pts',(63.0851797662401,-2.97397827264193,338.917223033777));
#61801=CARTESIAN_POINT('Ctrl Pts',(63.0774046874617,-2.86530777302618,338.999726302533));
#61802=CARTESIAN_POINT('Ctrl Pts',(63.0696296086832,-2.75302977802615,339.077834456283));
#61803=CARTESIAN_POINT('Ctrl Pts',(63.0618545299048,-2.63753533516603,339.151215535027));
#61804=CARTESIAN_POINT('Ctrl Pts',(63.0540890188558,-2.5221830155706,339.224506313682));
#61805=CARTESIAN_POINT('Ctrl Pts',(63.0463235078068,-2.4036224502484,339.293081383815));
#61806=CARTESIAN_POINT('Ctrl Pts',(63.0385579967578,-2.28227710740803,339.356649431329));
#61807=CARTESIAN_POINT('Ctrl Pts',(63.0308001852356,-2.16105207882837,339.42015445094));
#61808=CARTESIAN_POINT('Ctrl Pts',(63.0230423737133,-2.03704811151664,339.478662147309));
#61809=CARTESIAN_POINT('Ctrl Pts',(63.0152845621911,-1.91071665831261,339.53192507817));
#61810=CARTESIAN_POINT('Ctrl Pts',(63.0075325886681,-1.78448027353341,339.585147926986));
#61811=CARTESIAN_POINT('Ctrl Pts',(62.9997806151451,-1.65592024787204,339.63313371507));
#61812=CARTESIAN_POINT('Ctrl Pts',(62.9920286416221,-1.52551126140707,339.675681603127));
#61813=CARTESIAN_POINT('Ctrl Pts',(62.9842799510645,-1.39515750322539,339.718211472128));
#61814=CARTESIAN_POINT('Ctrl Pts',(62.9765312605069,-1.26295671246653,339.75530790053));
#61815=CARTESIAN_POINT('Ctrl Pts',(62.9687825699493,-1.12940190723566,339.786818817799));
#61816=CARTESIAN_POINT('Ctrl Pts',(62.9610354915714,-0.9958748891974,339.818323178958));
#61817=CARTESIAN_POINT('Ctrl Pts',(62.9532884131936,-0.860994797226269,
339.844244250806));
#61818=CARTESIAN_POINT('Ctrl Pts',(62.9455413348157,-0.725267728605298,
339.864480422855));
#61819=CARTESIAN_POINT('Ctrl Pts',(62.9377941915099,-0.589539522460763,
339.884716764504));
#61820=CARTESIAN_POINT('Ctrl Pts',(62.9300470482041,-0.452964712108936,
339.899268053682));
#61821=CARTESIAN_POINT('Ctrl Pts',(62.9222999048983,-0.316057062770399,
339.90808424903));
#61822=CARTESIAN_POINT('Ctrl Pts',(62.9145510198703,-0.179118633685938,
339.916902426445));
#61823=CARTESIAN_POINT('Ctrl Pts',(62.9068021348421,-0.041847606703032,
339.919982919211));
#61824=CARTESIAN_POINT('Ctrl Pts',(62.899053249814,0.0952400849282741,339.917327769096));
#61825=CARTESIAN_POINT('Ctrl Pts',(62.8912961400393,0.232473282852045,339.914669800777));
#61826=CARTESIAN_POINT('Ctrl Pts',(62.8835390302646,0.369522365286114,339.906264036064));
#61827=CARTESIAN_POINT('Ctrl Pts',(62.8757819204898,0.505873801834289,339.892164629192));
#61828=CARTESIAN_POINT('Ctrl Pts',(62.8680206655637,0.642298100230388,339.878057688048));
#61829=CARTESIAN_POINT('Ctrl Pts',(62.8602594106375,0.778023623322308,339.858251098702));
#61830=CARTESIAN_POINT('Ctrl Pts',(62.8524981557114,0.912545885136313,339.832850408405));
#61831=CARTESIAN_POINT('Ctrl Pts',(62.8447244853067,1.04728333872861,339.807409085281));
#61832=CARTESIAN_POINT('Ctrl Pts',(62.836950814902,1.18081330375572,339.77635586756));
#61833=CARTESIAN_POINT('Ctrl Pts',(62.8291771444974,1.31264446998372,339.739846786334));
#61834=CARTESIAN_POINT('Ctrl Pts',(62.8217653403203,1.43833886370653,339.705037211623));
#61835=CARTESIAN_POINT('Ctrl Pts',(62.8143535361432,1.56248878346954,339.665268371201));
#61836=CARTESIAN_POINT('Ctrl Pts',(62.8069417319662,1.68468612922753,339.620715930296));
#61837=CARTESIAN_POINT('Ctrl Pts',(62.7991666531877,1.81287273090878,339.573979841546));
#61838=CARTESIAN_POINT('Ctrl Pts',(62.7913915744093,1.93931560936574,339.521831684043));
#61839=CARTESIAN_POINT('Ctrl Pts',(62.7836164956309,2.06352399409944,339.46442065539));
#61840=CARTESIAN_POINT('Ctrl Pts',(62.7758509845819,2.18757953250806,339.407080274663));
#61841=CARTESIAN_POINT('Ctrl Pts',(62.7680854735329,2.30940569686697,339.34449007119));
#61842=CARTESIAN_POINT('Ctrl Pts',(62.7603199624839,2.42852835199182,339.276848501651));
#61843=CARTESIAN_POINT('Ctrl Pts',(62.7525621509617,2.54753289665754,339.209273998924));
#61844=CARTESIAN_POINT('Ctrl Pts',(62.7448043394394,2.66383892880011,339.136658288979));
#61845=CARTESIAN_POINT('Ctrl Pts',(62.7370465279172,2.7769940619019,339.059247102932));
#61846=CARTESIAN_POINT('Ctrl Pts',(62.7292945543942,2.89006404217744,338.981894171257));
#61847=CARTESIAN_POINT('Ctrl Pts',(62.7215425808713,2.99998752176656,338.899753166327));
#61848=CARTESIAN_POINT('Ctrl Pts',(62.7137906073483,3.1063387339954,338.81311457108));
#61849=CARTESIAN_POINT('Ctrl Pts',(62.7060419167907,3.21264490642279,338.726512667329));
#61850=CARTESIAN_POINT('Ctrl Pts',(62.698293226233,3.31538151804279,338.635417208001));
#61851=CARTESIAN_POINT('Ctrl Pts',(62.6905445356754,3.41415388911361,338.540160488445));
#61852=CARTESIAN_POINT('Ctrl Pts',(62.6827974572975,3.5129057097676,338.444923587846));
#61853=CARTESIAN_POINT('Ctrl Pts',(62.6750503789197,3.60769464926973,338.345527420295));
#61854=CARTESIAN_POINT('Ctrl Pts',(62.6673033005419,3.69816138291436,338.242342586529));
#61855=CARTESIAN_POINT('Ctrl Pts',(62.6595561572361,3.78862887475735,338.139156887975));
#61856=CARTESIAN_POINT('Ctrl Pts',(62.6518090139303,3.87477383080808,338.032182753782));
#61857=CARTESIAN_POINT('Ctrl Pts',(62.6440618706245,3.95627614237726,337.921825139832));
#61858=CARTESIAN_POINT('Ctrl Pts',(62.6363129855964,4.03779677739658,337.811442715148));
#61859=CARTESIAN_POINT('Ctrl Pts',(62.6285641005683,4.11467245879398,337.697675611404));
#61860=CARTESIAN_POINT('Ctrl Pts',(62.6208152155402,4.18662570244882,337.580958792793));
#61861=CARTESIAN_POINT('Ctrl Pts',(62.6130581057654,4.25865531801975,337.464118089745));
#61862=CARTESIAN_POINT('Ctrl Pts',(62.6053009959907,4.32575185352346,337.344321750904));
#61863=CARTESIAN_POINT('Ctrl Pts',(62.597543886216,4.38768294764708,337.222030920898));
#61864=CARTESIAN_POINT('Ctrl Pts',(62.5897826312898,4.44964713576718,337.099674742583));
#61865=CARTESIAN_POINT('Ctrl Pts',(62.5820213763637,4.50644022070559,336.974821772641));
#61866=CARTESIAN_POINT('Ctrl Pts',(62.5742601214375,4.55787795308787,336.847953361764));
#61867=CARTESIAN_POINT('Ctrl Pts',(62.5664864510329,4.60939796907848,336.720882002776));
#61868=CARTESIAN_POINT('Ctrl Pts',(62.5587127806282,4.65554538182932,336.591789128506));
#61869=CARTESIAN_POINT('Ctrl Pts',(62.5509391102236,4.69618552505608,336.461172329588));
#61870=CARTESIAN_POINT('Ctrl Pts',(62.5435273060464,4.7349338598383,336.336635774084));
#61871=CARTESIAN_POINT('Ctrl Pts',(62.5361155018693,4.76867603880182,336.210714256445));
#61872=CARTESIAN_POINT('Ctrl Pts',(62.5287036976922,4.79733893623155,336.083846019237));
#61873=CARTESIAN_POINT('Ctrl Pts',(62.5209286189138,4.82740668764666,335.950759591804));
#61874=CARTESIAN_POINT('Ctrl Pts',(62.5131535401353,4.85197968629453,335.816210717483));
#61875=CARTESIAN_POINT('Ctrl Pts',(62.5053784613569,4.87091781154455,335.680692835042));
#61876=CARTESIAN_POINT('Ctrl Pts',(62.4976129503079,4.88983263222578,335.545341715983));
#61877=CARTESIAN_POINT('Ctrl Pts',(62.4898474392589,4.90312632274071,335.409024344802));
#61878=CARTESIAN_POINT('Ctrl Pts',(62.4820819282098,4.91070918778971,335.272246828187));
#61879=CARTESIAN_POINT('Ctrl Pts',(62.4743241166877,4.91828453440588,335.135604926878));
#61880=CARTESIAN_POINT('Ctrl Pts',(62.4665663051655,4.92016030235625,334.99850417583));
#61881=CARTESIAN_POINT('Ctrl Pts',(62.4588084936434,4.91629831987537,334.861457975723));
#61882=CARTESIAN_POINT('Ctrl Pts',(62.4510565201203,4.91243924365874,334.724514907228));
#61883=CARTESIAN_POINT('Ctrl Pts',(62.4433045465973,4.90285102242474,334.587626697109));
#61884=CARTESIAN_POINT('Ctrl Pts',(62.4355525730743,4.88754752269653,334.451308578632));
#61885=CARTESIAN_POINT('Ctrl Pts',(62.4278038825167,4.87225050400953,334.315048190959));
#61886=CARTESIAN_POINT('Ctrl Pts',(62.4200551919591,4.85124306439688,334.179357802359));
#61887=CARTESIAN_POINT('Ctrl Pts',(62.4123065014014,4.82459105425371,334.044749131529));
#61888=CARTESIAN_POINT('Ctrl Pts',(62.4045594230236,4.79794458928388,333.910168467157));
#61889=CARTESIAN_POINT('Ctrl Pts',(62.3968123446458,4.76565596561848,333.776669456083));
#61890=CARTESIAN_POINT('Ctrl Pts',(62.3890652662679,4.72784237810801,333.644754815443));
#61891=CARTESIAN_POINT('Ctrl Pts',(62.3813181229621,4.69002847368325,333.512839069231));
#61892=CARTESIAN_POINT('Ctrl Pts',(62.3735709796563,4.64668962076268,333.382508095679));
#61893=CARTESIAN_POINT('Ctrl Pts',(62.3658238363505,4.59799312620769,333.254250225878));
#61894=CARTESIAN_POINT('Ctrl Pts',(62.3580749513224,4.54928568364693,333.125963520985));
#61895=CARTESIAN_POINT('Ctrl Pts',(62.3503260662943,4.49521834132334,332.999751212637));
#61896=CARTESIAN_POINT('Ctrl Pts',(62.3425771812662,4.43600670732754,332.876082027232));
#61897=CARTESIAN_POINT('Ctrl Pts',(62.3348200714915,4.37673222549155,332.752281578077));
#61898=CARTESIAN_POINT('Ctrl Pts',(62.3270629617168,4.31230271377637,332.63102999707));
#61899=CARTESIAN_POINT('Ctrl Pts',(62.319305851942,4.2429802144996,332.512772233617));
#61900=CARTESIAN_POINT('Ctrl Pts',(62.3115445970159,4.17362067149572,332.394451276997));
#61901=CARTESIAN_POINT('Ctrl Pts',(62.3037833420897,4.0993631424971,332.279127654147));
#61902=CARTESIAN_POINT('Ctrl Pts',(62.2960220871635,4.02051269766,332.167216790777));
#61903=CARTESIAN_POINT('Ctrl Pts',(62.2882484167588,3.94153611780852,332.055126906498));
#61904=CARTESIAN_POINT('Ctrl Pts',(62.2804747463542,3.85795217873632,331.946461000988));
#61905=CARTESIAN_POINT('Ctrl Pts',(62.2727010759495,3.77010643937014,331.841601592845));
#61906=CARTESIAN_POINT('Ctrl Pts',(62.2652892717725,3.68634994030634,331.741623415379));
#61907=CARTESIAN_POINT('Ctrl Pts',(62.2578774675954,3.59871967886907,331.645105538661));
#61908=CARTESIAN_POINT('Ctrl Pts',(62.2504656634184,3.50754461006283,331.552346613866));
#61909=CARTESIAN_POINT('Ctrl Pts',(62.2426905846399,3.41190077953747,331.455041297852));
#61910=CARTESIAN_POINT('Ctrl Pts',(62.2349155058615,3.31205362021402,331.36156522274));
#61911=CARTESIAN_POINT('Ctrl Pts',(62.2271404270831,3.20834224796475,331.272303246987));
#61912=CARTESIAN_POINT('Ctrl Pts',(62.2193749160341,3.10475849916148,331.183151113778));
#61913=CARTESIAN_POINT('Ctrl Pts',(62.2116094049851,2.99732029226123,331.09820301438));
#61914=CARTESIAN_POINT('Ctrl Pts',(62.2038438939361,2.8864046839016,331.017808258854));
#61915=CARTESIAN_POINT('Ctrl Pts',(62.1960860824139,2.77559904869134,330.937493214963));
#61916=CARTESIAN_POINT('Ctrl Pts',(62.1883282708917,2.66132318788856,330.861722758444));
#61917=CARTESIAN_POINT('Ctrl Pts',(62.1805704593696,2.54398817414573,330.790806819317));
#61918=CARTESIAN_POINT('Ctrl Pts',(62.1728184858466,2.42674145872108,330.719944246683));
#61919=CARTESIAN_POINT('Ctrl Pts',(62.1650665123236,2.30644050576853,330.653929121335));
#61920=CARTESIAN_POINT('Ctrl Pts',(62.1573145388006,2.18352608990462,330.593028604903));
#61921=CARTESIAN_POINT('Ctrl Pts',(62.149565848243,2.06066372836879,330.532153879875));
#61922=CARTESIAN_POINT('Ctrl Pts',(62.1418171576854,1.93519045478687,330.476389628835));
#61923=CARTESIAN_POINT('Ctrl Pts',(62.1340684671277,1.80757221975524,330.42595739713));
#61924=CARTESIAN_POINT('Ctrl Pts',(62.1263213887499,1.67998053676338,330.375535658272));
#61925=CARTESIAN_POINT('Ctrl Pts',(62.1185743103721,1.55024514328905,330.330443875696));
#61926=CARTESIAN_POINT('Ctrl Pts',(62.1108272319943,1.41885220575438,330.29085554684));
#61927=CARTESIAN_POINT('Ctrl Pts',(62.1030800886884,1.28745816701971,330.251266886196));
#61928=CARTESIAN_POINT('Ctrl Pts',(62.0953329453826,1.15440693077219,330.217181884032));
#61929=CARTESIAN_POINT('Ctrl Pts',(62.0875858020767,1.02019968438663,330.188724112413));
#61930=CARTESIAN_POINT('Ctrl Pts',(62.0798369170487,0.88596226536342,330.160259942883));
#61931=CARTESIAN_POINT('Ctrl Pts',(62.0720880320206,0.750568701336808,330.137425602411));
#61932=CARTESIAN_POINT('Ctrl Pts',(62.0643391469925,0.614529832246269,330.120293436304));
#61933=CARTESIAN_POINT('Ctrl Pts',(62.0565820372177,0.47834657009444,330.103143085939));
#61934=CARTESIAN_POINT('Ctrl Pts',(62.048824927443,0.34151702308346,330.091707048987));
#61935=CARTESIAN_POINT('Ctrl Pts',(62.0410678176683,0.204557164794303,330.086005756126));
#61936=CARTESIAN_POINT('Ctrl Pts',(62.0333065627421,0.0675241195359115,
330.080301416676));
#61937=CARTESIAN_POINT('Ctrl Pts',(62.025545307816,-0.0696389850770303,
330.080337927434));
#61938=CARTESIAN_POINT('Ctrl Pts',(62.0177840528898,-0.206417717737142,
330.086083559084));
#61939=CARTESIAN_POINT('Ctrl Pts',(62.0100103824852,-0.343415251793332,
330.091838381873));
#61940=CARTESIAN_POINT('Ctrl Pts',(62.0022367120805,-0.480026795498825,
330.103320542704));
#61941=CARTESIAN_POINT('Ctrl Pts',(61.9944630416758,-0.615743679042492,
330.120446456466));
#61942=CARTESIAN_POINT('Ctrl Pts',(61.9870512374987,-0.745142909006524,
330.136775154821));
#61943=CARTESIAN_POINT('Ctrl Pts',(61.9796394333216,-0.873728613345349,
330.158233949887));
#61944=CARTESIAN_POINT('Ctrl Pts',(61.9722276291444,-1.00107163348714,330.184707833669));
#61945=CARTESIAN_POINT('Ctrl Pts',(61.964452550366,-1.1346561143806,330.212479281356));
#61946=CARTESIAN_POINT('Ctrl Pts',(61.9566774715876,-1.26729516730605,330.245857619878));
#61947=CARTESIAN_POINT('Ctrl Pts',(61.9489023928091,-1.39848164151895,330.284765948457));
#61948=CARTESIAN_POINT('Ctrl Pts',(61.9411368817601,-1.52950668242314,330.32362639786));
#61949=CARTESIAN_POINT('Ctrl Pts',(61.9333713707111,-1.65908233005115,330.368003187231));
#61950=CARTESIAN_POINT('Ctrl Pts',(61.9256058596622,-1.78671079513906,330.417768273316));
#61951=CARTESIAN_POINT('Ctrl Pts',(61.91784804814,-1.91421271623269,330.467484017173));
#61952=CARTESIAN_POINT('Ctrl Pts',(61.9100902366177,-2.03977093503971,330.522577284761));
#61953=CARTESIAN_POINT('Ctrl Pts',(61.9023324250955,-2.16290236979551,330.582870117233));
#61954=CARTESIAN_POINT('Ctrl Pts',(61.8945804515725,-2.28594114424235,330.643117577437));
#61955=CARTESIAN_POINT('Ctrl Pts',(61.8868284780495,-2.40655642002873,330.708556643011));
#61956=CARTESIAN_POINT('Ctrl Pts',(61.8790765045264,-2.52428500680449,330.778961233663));
#61957=CARTESIAN_POINT('Ctrl Pts',(61.8713278139688,-2.6419637354533,330.849336007929));
#61958=CARTESIAN_POINT('Ctrl Pts',(61.8635791234112,-2.75675787182096,330.924671924549));
#61959=CARTESIAN_POINT('Ctrl Pts',(61.8558304328536,-2.86822896109472,331.004697046626));
#61960=CARTESIAN_POINT('Ctrl Pts',(61.8480833544758,-2.97967685787717,331.084705518808));
#61961=CARTESIAN_POINT('Ctrl Pts',(61.8403362760979,-3.08780276546037,331.169401028047));
#61962=CARTESIAN_POINT('Ctrl Pts',(61.8325891977201,-3.19219769360033,331.258468636043));
#61963=CARTESIAN_POINT('Ctrl Pts',(61.8248420544143,-3.29659349667041,331.347536990512));
#61964=CARTESIAN_POINT('Ctrl Pts',(61.8170949111085,-3.39725796057302,331.440977263128));
#61965=CARTESIAN_POINT('Ctrl Pts',(61.8093477678027,-3.4938159496763,331.53843486667));
#61966=CARTESIAN_POINT('Ctrl Pts',(61.8015988827747,-3.59039564706519,331.635914380749));
#61967=CARTESIAN_POINT('Ctrl Pts',(61.7938499977466,-3.68286675749314,331.73741274537));
#61968=CARTESIAN_POINT('Ctrl Pts',(61.7861011127185,-3.77089199944426,331.842539534527));
#61969=CARTESIAN_POINT('Ctrl Pts',(61.7783440029438,-3.85901067229702,331.947777906343));
#61970=CARTESIAN_POINT('Ctrl Pts',(61.7705868931691,-3.94267379891279,332.056652095761));
#61971=CARTESIAN_POINT('Ctrl Pts',(61.7628297833944,-4.02158497578674,332.168739265799));
#61972=CARTESIAN_POINT('Ctrl Pts',(61.7550685284682,-4.10053832027053,332.280886331638));
#61973=CARTESIAN_POINT('Ctrl Pts',(61.747307273542,-4.17473444391868,332.396249470619));
#61974=CARTESIAN_POINT('Ctrl Pts',(61.7395460186159,-4.24392164029049,332.51437891593));
#61975=CARTESIAN_POINT('Ctrl Pts',(61.7317723482112,-4.31321951362839,332.632697329855));
#61976=CARTESIAN_POINT('Ctrl Pts',(61.7239986778065,-4.37749226469182,332.753790547508));
#61977=CARTESIAN_POINT('Ctrl Pts',(61.7162250074019,-4.43653491156297,332.877185584894));
#61978=CARTESIAN_POINT('Ctrl Pts',(61.7088132032248,-4.49282910901754,332.994836553602));
#61979=CARTESIAN_POINT('Ctrl Pts',(61.7014013990477,-4.54436905330684,333.114579600951));
#61980=CARTESIAN_POINT('Ctrl Pts',(61.6939895948706,-4.59101921477869,333.235991600918));
#61981=CARTESIAN_POINT('Ctrl Pts',(61.6851310443183,-4.64677524985418,333.381102604077));
#61982=CARTESIAN_POINT('Ctrl Pts',(61.676272493766,-4.69569362969611,333.528978980461));
#61983=CARTESIAN_POINT('Ctrl Pts',(61.6674139432137,-4.73752685456457,333.679007053471));
#61984=CARTESIAN_POINT('Ctrl Pts',(61.6585852460574,-4.77921910108445,333.828529530509));
#61985=CARTESIAN_POINT('Ctrl Pts',(61.6497565489011,-4.81387375886097,333.980189069039));
#61986=CARTESIAN_POINT('Ctrl Pts',(61.6409278517448,-4.84129228426136,334.133355851083));
#61987=CARTESIAN_POINT('Ctrl Pts',(61.6321565567288,-4.86853254077153,334.28552677825));
#61988=CARTESIAN_POINT('Ctrl Pts',(61.623385261713,-4.88863036829126,334.439185241312));
#61989=CARTESIAN_POINT('Ctrl Pts',(61.6146139666971,-4.90143841270151,334.59369402048));
#61990=CARTESIAN_POINT('Ctrl Pts',(61.6070151033191,-4.91253444577709,334.727550093209));
#61991=CARTESIAN_POINT('Ctrl Pts',(61.5994162399411,-4.91815993583621,334.862043987869));
#61992=CARTESIAN_POINT('Ctrl Pts',(61.5918173765632,-4.91824892677099,334.996750874583));
#61993=CARTESIAN_POINT('',(59.841817376455,-4.9182486281821,335.003673402358));
#61994=CARTESIAN_POINT('Ctrl Pts',(61.5918173765087,-4.91824892677163,334.996750875548));
#61995=CARTESIAN_POINT('Ctrl Pts',(61.5840252789637,-4.91834018066105,335.134883271021));
#61996=CARTESIAN_POINT('Ctrl Pts',(61.5762331814186,-4.91260779228916,335.273048117306));
#61997=CARTESIAN_POINT('Ctrl Pts',(61.5684410838736,-4.90107024508939,335.410723161265));
#61998=CARTESIAN_POINT('Ctrl Pts',(61.5606487003074,-4.88953227438594,335.548403258801));
#61999=CARTESIAN_POINT('Ctrl Pts',(61.5528563167414,-4.87218875192799,335.685593135114));
#62000=CARTESIAN_POINT('Ctrl Pts',(61.5450639331752,-4.84911011845927,335.821774982313));
#62001=CARTESIAN_POINT('Ctrl Pts',(61.5372696505982,-4.82602586070693,335.95799001715));
#62002=CARTESIAN_POINT('Ctrl Pts',(61.5294753680212,-4.79720377335317,336.093196154834));
#62003=CARTESIAN_POINT('Ctrl Pts',(61.5216810854442,-4.76276550273706,336.226885417811));
#62004=CARTESIAN_POINT('Ctrl Pts',(61.5138832899863,-4.72831171080222,336.360634934501));
#62005=CARTESIAN_POINT('Ctrl Pts',(61.5060854945284,-4.68823679188107,336.492865843505));
#62006=CARTESIAN_POINT('Ctrl Pts',(61.4982876990705,-4.64271227470297,336.623085270965));
#62007=CARTESIAN_POINT('Ctrl Pts',(61.4904799396305,-4.59712958653596,336.753471092124));
#62008=CARTESIAN_POINT('Ctrl Pts',(61.4826721801905,-4.54608352075104,336.881839935816));
#62009=CARTESIAN_POINT('Ctrl Pts',(61.4748644207505,-4.48979403191505,337.007718260484));
#62010=CARTESIAN_POINT('Ctrl Pts',(61.4670510735764,-4.43346425870533,337.133686671766));
#62011=CARTESIAN_POINT('Ctrl Pts',(61.4592377264023,-4.37188375645724,337.2571606695));
#62012=CARTESIAN_POINT('Ctrl Pts',(61.4514243792281,-4.30531805861462,337.377692048325));
#62013=CARTESIAN_POINT('Ctrl Pts',(61.4435985258357,-4.2386458142272,337.498416352371));
#62014=CARTESIAN_POINT('Ctrl Pts',(61.4357726724433,-4.16697263647571,337.616188302863));
#62015=CARTESIAN_POINT('Ctrl Pts',(61.427946819051,-4.09060730540156,337.73058875254));
#62016=CARTESIAN_POINT('Ctrl Pts',(61.4238817328995,-4.0509398551901,337.790013285608));
#62017=CARTESIAN_POINT('Ctrl Pts',(61.4198166467479,-4.01000702988523,337.848528657322));
#62018=CARTESIAN_POINT('Ctrl Pts',(61.4157515605964,-3.96785622599952,337.906079839285));
#62019=CARTESIAN_POINT('Ctrl Pts',(61.407976481818,-3.88723657648375,338.016154990678));
#62020=CARTESIAN_POINT('Ctrl Pts',(61.4002014030395,-3.80190555086133,338.12304674859));
#62021=CARTESIAN_POINT('Ctrl Pts',(61.3924263242611,-3.71214325095125,338.226325393837));
#62022=CARTESIAN_POINT('Ctrl Pts',(61.3846608132121,-3.62249140926588,338.329476948136));
#62023=CARTESIAN_POINT('Ctrl Pts',(61.3768953021631,-3.52841939708857,338.429023944163));
#62024=CARTESIAN_POINT('Ctrl Pts',(61.3691297911141,-3.4302499846955,338.5245663712));
#62025=CARTESIAN_POINT('Ctrl Pts',(61.361371979592,-3.33217790756069,338.620014067643));
#62026=CARTESIAN_POINT('Ctrl Pts',(61.3536141680697,-3.23001679329037,338.711464825838));
#62027=CARTESIAN_POINT('Ctrl Pts',(61.3458563565476,-3.12412874913807,338.798552700873));
#62028=CARTESIAN_POINT('Ctrl Pts',(61.3381043830245,-3.01832038909653,338.88557503952));
#62029=CARTESIAN_POINT('Ctrl Pts',(61.3303524095015,-2.90879098232934,338.968240782784));
#62030=CARTESIAN_POINT('Ctrl Pts',(61.3226004359785,-2.79593819245683,339.046222026343));
#62031=CARTESIAN_POINT('Ctrl Pts',(61.3148517454209,-2.68313319580806,339.124170244799));
#62032=CARTESIAN_POINT('Ctrl Pts',(61.3071030548632,-2.56700793628352,339.197437687621));
#62033=CARTESIAN_POINT('Ctrl Pts',(61.2993543643056,-2.44799156563884,339.265737961603));
#62034=CARTESIAN_POINT('Ctrl Pts',(61.2916072859278,-2.32899995734421,339.334024025142));
#62035=CARTESIAN_POINT('Ctrl Pts',(61.28386020755,-2.20711877319843,339.397344781037));
#62036=CARTESIAN_POINT('Ctrl Pts',(61.2761131291721,-2.08280409522519,339.455458468375));
#62037=CARTESIAN_POINT('Ctrl Pts',(61.2683659858663,-1.95848837537512,339.513572642762));
#62038=CARTESIAN_POINT('Ctrl Pts',(61.2606188425605,-1.83173947511246,339.566479496019));
#62039=CARTESIAN_POINT('Ctrl Pts',(61.2528716992547,-1.70303553671758,339.61398450617));
#62040=CARTESIAN_POINT('Ctrl Pts',(61.2451228142266,-1.57430266294463,339.661500196456));
#62041=CARTESIAN_POINT('Ctrl Pts',(61.2373739291985,-1.44361424303709,339.703611491697));
#62042=CARTESIAN_POINT('Ctrl Pts',(61.2296250441704,-1.3114653547824,339.740173170434));
#62043=CARTESIAN_POINT('Ctrl Pts',(61.2218679343956,-1.17917620233272,339.776773656116));
#62044=CARTESIAN_POINT('Ctrl Pts',(61.2141108246209,-1.04542386227026,339.807812654235));
#62045=CARTESIAN_POINT('Ctrl Pts',(61.2063537148462,-0.910715975303693,
339.833195575892));
#62046=CARTESIAN_POINT('Ctrl Pts',(61.19859245992,-0.77593610474936,339.858592061372));
#62047=CARTESIAN_POINT('Ctrl Pts',(61.1908312049939,-0.640200056458475,
339.878326391725));
#62048=CARTESIAN_POINT('Ctrl Pts',(61.1830699500677,-0.504021463225214,
339.892355815669));
#62049=CARTESIAN_POINT('Ctrl Pts',(61.175296279663,-0.367625028623465,339.906407682119));
#62050=CARTESIAN_POINT('Ctrl Pts',(61.1675226092584,-0.230785024787696,
339.914736381967));
#62051=CARTESIAN_POINT('Ctrl Pts',(61.1597489388537,-0.0940168575877119,
339.917351308681));
#62052=CARTESIAN_POINT('Ctrl Pts',(61.1523371346767,0.0363847185236617,
339.919844509927));
#62053=CARTESIAN_POINT('Ctrl Pts',(61.1449253304996,0.166720707746468,339.917143925025));
#62054=CARTESIAN_POINT('Ctrl Pts',(61.1375135263226,0.29654985591658,339.909301502806));
#62055=CARTESIAN_POINT('Ctrl Pts',(61.1297384475442,0.432742317380743,339.901074700113));
#62056=CARTESIAN_POINT('Ctrl Pts',(61.1219633687657,0.568807391302568,339.887163283864));
#62057=CARTESIAN_POINT('Ctrl Pts',(61.1141882899873,0.704232138484992,339.867570251945));
#62058=CARTESIAN_POINT('Ctrl Pts',(61.1064227789383,0.839490236894263,339.8480013305));
#62059=CARTESIAN_POINT('Ctrl Pts',(61.0986572678893,0.974109193235749,339.822764760078));
#62060=CARTESIAN_POINT('Ctrl Pts',(61.0908917568403,1.10757796044543,339.791915496337));
#62061=CARTESIAN_POINT('Ctrl Pts',(61.0831339453181,1.24091439298383,339.761096819731));
#62062=CARTESIAN_POINT('Ctrl Pts',(61.0753761337959,1.37310252750178,339.724676611932));
#62063=CARTESIAN_POINT('Ctrl Pts',(61.0676183222737,1.5036386761024,339.682761342865));
#62064=CARTESIAN_POINT('Ctrl Pts',(61.0598663487507,1.63407659211166,339.640877616366));
#62065=CARTESIAN_POINT('Ctrl Pts',(61.0521143752277,1.76286462601576,339.593507178548));
#62066=CARTESIAN_POINT('Ctrl Pts',(61.0443624017047,1.8895118374728,339.540806985388));
#62067=CARTESIAN_POINT('Ctrl Pts',(61.036613711147,2.01610541376061,339.488129110792));
#62068=CARTESIAN_POINT('Ctrl Pts',(61.0288650205894,2.14055961071737,339.43012612003));
#62069=CARTESIAN_POINT('Ctrl Pts',(61.0211163300318,2.26240135554464,339.367003912172));
#62070=CARTESIAN_POINT('Ctrl Pts',(61.013369251654,2.38421775017934,339.303894837417));
#62071=CARTESIAN_POINT('Ctrl Pts',(61.0056221732762,2.50342242698248,339.235668843807));
#62072=CARTESIAN_POINT('Ctrl Pts',(60.9978750948983,2.61956527189246,339.162578629743));
#62073=CARTESIAN_POINT('Ctrl Pts',(60.9901279515925,2.73570909019103,339.089487803113));
#62074=CARTESIAN_POINT('Ctrl Pts',(60.9823808082867,2.84879069459559,339.011532882906));
#62075=CARTESIAN_POINT('Ctrl Pts',(60.9746336649809,2.95838775720216,338.929010682161));
#62076=CARTESIAN_POINT('Ctrl Pts',(60.9668847799529,3.06800945955507,338.846469928674));
#62077=CARTESIAN_POINT('Ctrl Pts',(60.9591358949248,3.17414474903934,338.759360086459));
#62078=CARTESIAN_POINT('Ctrl Pts',(60.9513870098967,3.27640359083491,338.668018889328));
#62079=CARTESIAN_POINT('Ctrl Pts',(60.943629900122,3.37877097122196,338.576580741705));
#62080=CARTESIAN_POINT('Ctrl Pts',(60.9358727903473,3.47725339284377,338.480902528365));
#62081=CARTESIAN_POINT('Ctrl Pts',(60.9281156805725,3.57149660036133,338.381359947729));
#62082=CARTESIAN_POINT('Ctrl Pts',(60.9203544256464,3.66579016843575,338.281764174721));
#62083=CARTESIAN_POINT('Ctrl Pts',(60.9125931707202,3.75583975210618,338.178300214421));
#62084=CARTESIAN_POINT('Ctrl Pts',(60.904831915794,3.8413314447297,338.071376856433));
#62085=CARTESIAN_POINT('Ctrl Pts',(60.8970582453894,3.92695989619969,337.964282455918));
#62086=CARTESIAN_POINT('Ctrl Pts',(60.8892845749847,4.00801565554107,337.853717914728));
#62087=CARTESIAN_POINT('Ctrl Pts',(60.8815109045801,4.08422770622956,337.740121731998));
#62088=CARTESIAN_POINT('Ctrl Pts',(60.874099100403,4.15689206762335,337.631813478903));
#62089=CARTESIAN_POINT('Ctrl Pts',(60.8666872962258,4.2251533706113,337.520749723517));
#62090=CARTESIAN_POINT('Ctrl Pts',(60.8592754920487,4.28881651212754,337.407329638376));
#62091=CARTESIAN_POINT('Ctrl Pts',(60.8515004132702,4.35559997385188,337.288350497001));
#62092=CARTESIAN_POINT('Ctrl Pts',(60.8437253344918,4.41753418605225,337.16640220795));
#62093=CARTESIAN_POINT('Ctrl Pts',(60.8359502557134,4.47434408888371,337.041917735065));
#62094=CARTESIAN_POINT('Ctrl Pts',(60.8281847446644,4.531084083513,336.917586448249));
#62095=CARTESIAN_POINT('Ctrl Pts',(60.8204192336153,4.58271215475666,336.790725539562));
#62096=CARTESIAN_POINT('Ctrl Pts',(60.8126537225663,4.62899795911042,336.661794499044));
#62097=CARTESIAN_POINT('Ctrl Pts',(60.8048959110441,4.67523787095444,336.532991294027));
#62098=CARTESIAN_POINT('Ctrl Pts',(60.7971380995219,4.71614592576654,336.40212240737));
#62099=CARTESIAN_POINT('Ctrl Pts',(60.7893802879997,4.75153908195503,336.269669017955));
#62100=CARTESIAN_POINT('Ctrl Pts',(60.7816283144767,4.78690560367109,336.137315303916));
#62101=CARTESIAN_POINT('Ctrl Pts',(60.7738763409537,4.81676538690688,336.003379836615));
#62102=CARTESIAN_POINT('Ctrl Pts',(60.7661243674307,4.84098474330442,335.868360396145));
#62103=CARTESIAN_POINT('Ctrl Pts',(60.7583756768731,4.86519384279014,335.73339813649));
#62104=CARTESIAN_POINT('Ctrl Pts',(60.7506269863155,4.8837671975729,335.597353200643));
#62105=CARTESIAN_POINT('Ctrl Pts',(60.7428782957579,4.89662194573607,335.460734829415));
#62106=CARTESIAN_POINT('Ctrl Pts',(60.7351312173801,4.90947401936153,335.32414488278));
#62107=CARTESIAN_POINT('Ctrl Pts',(60.7273841390022,4.91660981637787,335.186982126987));
#62108=CARTESIAN_POINT('Ctrl Pts',(60.7196370606244,4.9179982537162,335.049761822157));
#62109=CARTESIAN_POINT('Ctrl Pts',(60.7118899173186,4.91938670269097,334.91254036729));
#62110=CARTESIAN_POINT('Ctrl Pts',(60.7041427740128,4.91502769195745,334.775261753279));
#62111=CARTESIAN_POINT('Ctrl Pts',(60.696395630707,4.904942272072,334.638441747237));
#62112=CARTESIAN_POINT('Ctrl Pts',(60.6886467456789,4.89485458477002,334.501590981152));
#62113=CARTESIAN_POINT('Ctrl Pts',(60.6808978606508,4.87903795522636,334.365199417943));
#62114=CARTESIAN_POINT('Ctrl Pts',(60.6731489756227,4.85756532078576,334.229777813355));
#62115=CARTESIAN_POINT('Ctrl Pts',(60.665391865848,4.83606989506913,334.094212470877));
#62116=CARTESIAN_POINT('Ctrl Pts',(60.6576347560733,4.80890653352618,333.959619530252));
#62117=CARTESIAN_POINT('Ctrl Pts',(60.6498776462985,4.77619946108342,333.826500204326));
#62118=CARTESIAN_POINT('Ctrl Pts',(60.6421163913724,4.74347491102684,333.693309743688));
#62119=CARTESIAN_POINT('Ctrl Pts',(60.6343551364462,4.70520085627216,333.561594841977));
#62120=CARTESIAN_POINT('Ctrl Pts',(60.62659388152,4.66155118382066,333.431840689496));
#62121=CARTESIAN_POINT('Ctrl Pts',(60.6188202111154,4.6178316861187,333.301878972658));
#62122=CARTESIAN_POINT('Ctrl Pts',(60.6110465407107,4.5687195269991,333.173884637949));
#62123=CARTESIAN_POINT('Ctrl Pts',(60.6032728703061,4.51443678714722,333.04832288599));
#62124=CARTESIAN_POINT('Ctrl Pts',(60.5958610661289,4.46268092189494,332.928606063792));
#62125=CARTESIAN_POINT('Ctrl Pts',(60.5884492619519,4.40622514842957,332.811100706942));
#62126=CARTESIAN_POINT('Ctrl Pts',(60.5810374577747,4.34529955798734,332.696186896935));
#62127=CARTESIAN_POINT('Ctrl Pts',(60.5732623789963,4.28138782286967,332.575640818788));
#62128=CARTESIAN_POINT('Ctrl Pts',(60.5654873002178,4.21235506095974,332.457565801843));
#62129=CARTESIAN_POINT('Ctrl Pts',(60.5577122214394,4.13841651012453,332.342427451371));
#62130=CARTESIAN_POINT('Ctrl Pts',(60.5499467103904,4.06456894538324,332.227430785968));
#62131=CARTESIAN_POINT('Ctrl Pts',(60.5421811993413,3.98582781257757,332.115363922454));
#62132=CARTESIAN_POINT('Ctrl Pts',(60.5344156882923,3.90245485459703,332.006669218023));
#62133=CARTESIAN_POINT('Ctrl Pts',(60.5266578767701,3.81916456114723,331.898082284707));
#62134=CARTESIAN_POINT('Ctrl Pts',(60.5189000652479,3.73125181815416,331.792861164855));
#62135=CARTESIAN_POINT('Ctrl Pts',(60.5111422537257,3.63902220489834,331.69142017555));
#62136=CARTESIAN_POINT('Ctrl Pts',(60.5033902802027,3.54686199735138,331.590055523806));
#62137=CARTESIAN_POINT('Ctrl Pts',(60.4956383066798,3.45039164757307,331.492465628481));
#62138=CARTESIAN_POINT('Ctrl Pts',(60.4878863331568,3.34995740302223,331.399032288337));
#62139=CARTESIAN_POINT('Ctrl Pts',(60.4801376425991,3.24956569243358,331.305638517269));
#62140=CARTESIAN_POINT('Ctrl Pts',(60.4723889520415,3.14521371150051,331.216398065943));
#62141=CARTESIAN_POINT('Ctrl Pts',(60.4646402614839,3.03728485034606,331.131656194137));
#62142=CARTESIAN_POINT('Ctrl Pts',(60.4568931831061,2.92937844469239,331.046931953585));
#62143=CARTESIAN_POINT('Ctrl Pts',(60.4491461047282,2.81789694632411,330.966704672081));
#62144=CARTESIAN_POINT('Ctrl Pts',(60.4413990263504,2.70325682763859,330.89127932486));
#62145=CARTESIAN_POINT('Ctrl Pts',(60.4336518830446,2.58861574815877,330.815853345501));
#62146=CARTESIAN_POINT('Ctrl Pts',(60.4259047397388,2.47081632209832,330.745229595536));
#62147=CARTESIAN_POINT('Ctrl Pts',(60.418157596433,2.35030366068907,330.679669484281));
#62148=CARTESIAN_POINT('Ctrl Pts',(60.410408711405,2.22976390547539,330.614094633721));
#62149=CARTESIAN_POINT('Ctrl Pts',(60.4026598263769,2.10651004438315,330.553585873939));
#62150=CARTESIAN_POINT('Ctrl Pts',(60.3949109413488,1.98101105339722,330.498358269607));
#62151=CARTESIAN_POINT('Ctrl Pts',(60.3871538315741,1.85537885648518,330.443072046124));
#62152=CARTESIAN_POINT('Ctrl Pts',(60.3793967217994,1.72749712773497,330.393078333237));
#62153=CARTESIAN_POINT('Ctrl Pts',(60.3716396120246,1.5978545729571,330.348543902585));
#62154=CARTESIAN_POINT('Ctrl Pts',(60.3638783570985,1.46814274134284,330.303985674157));
#62155=CARTESIAN_POINT('Ctrl Pts',(60.3561171021723,1.33666858328727,330.264892652226));
#62156=CARTESIAN_POINT('Ctrl Pts',(60.3483558472462,1.20393420590136,330.231381175816));
#62157=CARTESIAN_POINT('Ctrl Pts',(60.3405821768415,1.07098749676984,330.197816091965));
#62158=CARTESIAN_POINT('Ctrl Pts',(60.3328085064368,0.936776922719063,330.169850475507));
#62159=CARTESIAN_POINT('Ctrl Pts',(60.3250348360322,0.801813861477001,330.147549320803));
#62160=CARTESIAN_POINT('Ctrl Pts',(60.3176230318551,0.673133363205629,330.126286290215));
#62161=CARTESIAN_POINT('Ctrl Pts',(60.310211227678,0.543769143310523,330.110172263506));
#62162=CARTESIAN_POINT('Ctrl Pts',(60.3027994235009,0.414165335998664,330.099219435951));
#62163=CARTESIAN_POINT('Ctrl Pts',(60.2950243447224,0.27820926002092,330.087729777691));
#62164=CARTESIAN_POINT('Ctrl Pts',(60.287249265944,0.141559870683655,330.081883733119));
#62165=CARTESIAN_POINT('Ctrl Pts',(60.2794741871656,0.00472518295217616,
330.081752269848));
#62166=CARTESIAN_POINT('Ctrl Pts',(60.2717086761166,-0.131941120984726,
330.081620968351));
#62167=CARTESIAN_POINT('Ctrl Pts',(60.2639431650675,-0.268791882480986,
330.087190256553));
#62168=CARTESIAN_POINT('Ctrl Pts',(60.2561776540185,-0.405313469839718,
330.098479414134));
#62169=CARTESIAN_POINT('Ctrl Pts',(60.2484198424964,-0.541699695646555,
330.109757378483));
#62170=CARTESIAN_POINT('Ctrl Pts',(60.2406620309742,-0.677757009789399,
330.126743894063));
#62171=CARTESIAN_POINT('Ctrl Pts',(60.232904219452,-0.812971637710933,330.149406203486));
#62172=CARTESIAN_POINT('Ctrl Pts',(60.225152245929,-0.94808451233687,330.172051458803));
#62173=CARTESIAN_POINT('Ctrl Pts',(60.2174002724061,-1.08235557903715,330.200363941969));
#62174=CARTESIAN_POINT('Ctrl Pts',(60.2096482988831,-1.21527640071851,330.234259099326));
#62175=CARTESIAN_POINT('Ctrl Pts',(60.2018996083255,-1.34814093035378,330.268139902064));
#62176=CARTESIAN_POINT('Ctrl Pts',(60.1941509177679,-1.47965597433335,330.307598580255));
#62177=CARTESIAN_POINT('Ctrl Pts',(60.1864022272102,-1.60932372195161,330.352499572839));
#62178=CARTESIAN_POINT('Ctrl Pts',(60.1786551488324,-1.73896449111171,330.397391223396));
#62179=CARTESIAN_POINT('Ctrl Pts',(60.1709080704546,-1.86675835927599,330.447722808265));
#62180=CARTESIAN_POINT('Ctrl Pts',(60.1631609920767,-1.99222348915277,330.50330914652));
#62181=CARTESIAN_POINT('Ctrl Pts',(60.1554138487709,-2.11768967054852,330.558895950643));
#62182=CARTESIAN_POINT('Ctrl Pts',(60.1476667054651,-2.24082671735732,330.619737437661));
#62183=CARTESIAN_POINT('Ctrl Pts',(60.1399195621593,-2.36117392967945,330.685600767627));
#62184=CARTESIAN_POINT('Ctrl Pts',(60.1321706771312,-2.48154819860988,330.751478905067));
#62185=CARTESIAN_POINT('Ctrl Pts',(60.1244217921031,-2.59913104215112,330.822380944456));
#62186=CARTESIAN_POINT('Ctrl Pts',(60.116672907075,-2.71348781801745,330.898028897716));
#62187=CARTESIAN_POINT('Ctrl Pts',(60.1089157973002,-2.82796597334706,330.973757144496));
#62188=CARTESIAN_POINT('Ctrl Pts',(60.1011586875255,-2.93921089436184,331.054241151757));
#62189=CARTESIAN_POINT('Ctrl Pts',(60.0934015777507,-3.04681787247629,331.139160206061));
#62190=CARTESIAN_POINT('Ctrl Pts',(60.0856403228246,-3.15448235231953,331.224124638394));
#62191=CARTESIAN_POINT('Ctrl Pts',(60.0778790678984,-3.25850471938399,331.313528585457));
#62192=CARTESIAN_POINT('Ctrl Pts',(60.0701178129722,-3.35851542273365,331.407012772391));
#62193=CARTESIAN_POINT('Ctrl Pts',(60.0623441425675,-3.45868611061499,331.500646503558));
#62194=CARTESIAN_POINT('Ctrl Pts',(60.0545704721628,-3.55483203673541,331.598373238802));
#62195=CARTESIAN_POINT('Ctrl Pts',(60.0467968017582,-3.64662181011738,331.69979812186));
#62196=CARTESIAN_POINT('Ctrl Pts',(60.0393849975811,-3.73413874746507,331.796501652211));
#62197=CARTESIAN_POINT('Ctrl Pts',(60.031973193404,-3.8176957786048,331.896566560111));
#62198=CARTESIAN_POINT('Ctrl Pts',(60.0245613892269,-3.89704230176514,331.999625963192));
#62199=CARTESIAN_POINT('Ctrl Pts',(60.016776715821,-3.98038054896428,332.107870025667));
#62200=CARTESIAN_POINT('Ctrl Pts',(60.008992042415,-4.05934074947212,332.219764549991));
#62201=CARTESIAN_POINT('Ctrl Pts',(60.0012073690091,-4.13358642093639,332.334920946172));
#62202=CARTESIAN_POINT('Ctrl Pts',(59.9934321517147,-4.20774190552753,332.449937460862));
#62203=CARTESIAN_POINT('Ctrl Pts',(59.9856569344203,-4.2771940441256,332.568207642411));
#62204=CARTESIAN_POINT('Ctrl Pts',(59.9778817171259,-4.34164653907798,332.689309974875));
#62205=CARTESIAN_POINT('Ctrl Pts',(59.9701142788049,-4.40603455039957,332.810291146505));
#62206=CARTESIAN_POINT('Ctrl Pts',(59.9623468404838,-4.46543268857561,332.934098490605));
#62207=CARTESIAN_POINT('Ctrl Pts',(59.9545794021628,-4.51958814211101,333.060281956523));
#62208=CARTESIAN_POINT('Ctrl Pts',(59.9468180714008,-4.57370101305762,333.186366204019));
#62209=CARTESIAN_POINT('Ctrl Pts',(59.9390567406389,-4.62257925027931,333.314822499283));
#62210=CARTESIAN_POINT('Ctrl Pts',(59.9312954098769,-4.66601633569451,333.445176981926));
#62211=CARTESIAN_POINT('Ctrl Pts',(59.9235382621031,-4.70943001058681,333.575461209703));
#62212=CARTESIAN_POINT('Ctrl Pts',(59.9157811143292,-4.74740824704905,333.707641220669));
#62213=CARTESIAN_POINT('Ctrl Pts',(59.9080239665553,-4.77979308485661,333.841224297607));
#62214=CARTESIAN_POINT('Ctrl Pts',(59.9002694187959,-4.81216706802442,333.974762600624));
#62215=CARTESIAN_POINT('Ctrl Pts',(59.8925148710364,-4.83895129421285,334.109702655429));
#62216=CARTESIAN_POINT('Ctrl Pts',(59.884760323277,-4.86003810017957,334.245538120709));
#62217=CARTESIAN_POINT('Ctrl Pts',(59.8770048338147,-4.88112746690225,334.381390081682));
#62218=CARTESIAN_POINT('Ctrl Pts',(59.8692493443525,-4.89651796439513,334.518137286886));
#62219=CARTESIAN_POINT('Ctrl Pts',(59.8614938548903,-4.90615334902285,334.655264770625));
#62220=CARTESIAN_POINT('Ctrl Pts',(59.8549350287631,-4.91430200459762,334.771233637256));
#62221=CARTESIAN_POINT('Ctrl Pts',(59.8483762026358,-4.91833541644559,334.887474215136));
#62222=CARTESIAN_POINT('Ctrl Pts',(59.8418173765087,-4.91824862818281,335.003673401407));
#62223=CARTESIAN_POINT('',(58.0918173765376,-4.9182497400553,335.001599045328));
#62224=CARTESIAN_POINT('Ctrl Pts',(59.841817376455,-4.9182486281821,335.003673402358));
#62225=CARTESIAN_POINT('Ctrl Pts',(59.8328697105503,-4.91813023007766,335.16219437501));
#62226=CARTESIAN_POINT('Ctrl Pts',(59.8239220446457,-4.91034393130489,335.320402619854));
#62227=CARTESIAN_POINT('Ctrl Pts',(59.8149743787411,-4.89500389926988,335.47761897851));
#62228=CARTESIAN_POINT('Ctrl Pts',(59.8059790090573,-4.87958208305695,335.635673523854));
#62229=CARTESIAN_POINT('Ctrl Pts',(59.7969836393734,-4.85652588434234,335.792725455033));
#62230=CARTESIAN_POINT('Ctrl Pts',(59.7879882696896,-4.82600062916286,335.948103891891));
#62231=CARTESIAN_POINT('Ctrl Pts',(59.7789342593916,-4.79527638052607,336.104495237312));
#62232=CARTESIAN_POINT('Ctrl Pts',(59.7698802490936,-4.75698546075449,336.259191077032));
#62233=CARTESIAN_POINT('Ctrl Pts',(59.7608262387955,-4.71134483422381,336.411528574111));
#62234=CARTESIAN_POINT('Ctrl Pts',(59.7559919441813,-4.6869754964648,336.492867595985));
#62235=CARTESIAN_POINT('Ctrl Pts',(59.7511576495671,-4.66051163143577,336.573534645542));
#62236=CARTESIAN_POINT('Ctrl Pts',(59.7463233549529,-4.63199173944947,336.653431458565));
#62237=CARTESIAN_POINT('Ctrl Pts',(59.7385482761745,-4.58612270898243,336.781930870572));
#62238=CARTESIAN_POINT('Ctrl Pts',(59.730773197396,-4.53482995317445,336.908723161525));
#62239=CARTESIAN_POINT('Ctrl Pts',(59.7229981186176,-4.47825935071902,337.033316564187));
#62240=CARTESIAN_POINT('Ctrl Pts',(59.7152326075686,-4.42175836199133,337.157756646736));
#62241=CARTESIAN_POINT('Ctrl Pts',(59.7074670965196,-4.35999260931081,337.280002872399));
#62242=CARTESIAN_POINT('Ctrl Pts',(59.6997015854705,-4.29315734170597,337.399579776097));
#62243=CARTESIAN_POINT('Ctrl Pts',(59.6919437739483,-4.22638834146355,337.519038118948));
#62244=CARTESIAN_POINT('Ctrl Pts',(59.6841859624261,-4.15456001867061,337.635832067799));
#62245=CARTESIAN_POINT('Ctrl Pts',(59.6764281509039,-4.07791504264166,337.749507586368));
#62246=CARTESIAN_POINT('Ctrl Pts',(59.6686761773809,-4.00132774438777,337.863097560505));
#62247=CARTESIAN_POINT('Ctrl Pts',(59.6609242038579,-3.91993122529002,337.973573452603));
#62248=CARTESIAN_POINT('Ctrl Pts',(59.6531722303349,-3.83401308530189,338.080507543285));
#62249=CARTESIAN_POINT('Ctrl Pts',(59.6454235397773,-3.74813133169705,338.187396347315));
#62250=CARTESIAN_POINT('Ctrl Pts',(59.6376748492196,-3.65773201013273,338.290746029164));
#62251=CARTESIAN_POINT('Ctrl Pts',(59.629926158662,-3.56314474203457,338.390159673203));
#62252=CARTESIAN_POINT('Ctrl Pts',(59.6221790802842,-3.46857715360755,338.489552633403));
#62253=CARTESIAN_POINT('Ctrl Pts',(59.6144320019064,-3.3698236210594,338.585010901694));
#62254=CARTESIAN_POINT('Ctrl Pts',(59.6066849235285,-3.26725230917648,338.676172657899));
#62255=CARTESIAN_POINT('Ctrl Pts',(59.5989377802227,-3.16468013764717,338.767335178126));
#62256=CARTESIAN_POINT('Ctrl Pts',(59.5911906369169,-3.05829041512443,338.854200854782));
#62257=CARTESIAN_POINT('Ctrl Pts',(59.5834434936111,-2.94848592568758,338.936446850717));
#62258=CARTESIAN_POINT('Ctrl Pts',(59.575694608583,-2.8386567498703,339.018711337298));
#62259=CARTESIAN_POINT('Ctrl Pts',(59.5679457235549,-2.72541159226266,339.096353842172));
#62260=CARTESIAN_POINT('Ctrl Pts',(59.5601968385268,-2.60918353253,339.169093949058));
#62261=CARTESIAN_POINT('Ctrl Pts',(59.552439728752,-2.49283210713396,339.241911263045));
#62262=CARTESIAN_POINT('Ctrl Pts',(59.5446826189773,-2.37349178692383,339.309815576962));
#62263=CARTESIAN_POINT('Ctrl Pts',(59.5369255092025,-2.25162213623948,339.372571419439));
#62264=CARTESIAN_POINT('Ctrl Pts',(59.5291642542764,-2.12968736231044,339.435360796632));
#62265=CARTESIAN_POINT('Ctrl Pts',(59.5214029993502,-2.00522091924836,339.492996056252));
#62266=CARTESIAN_POINT('Ctrl Pts',(59.513641744424,-1.87870290202377,339.545289701265));
#62267=CARTESIAN_POINT('Ctrl Pts',(59.5058680740194,-1.75198249720375,339.597666999067));
#62268=CARTESIAN_POINT('Ctrl Pts',(59.4980944036147,-1.6232043274728,339.644685473008));
#62269=CARTESIAN_POINT('Ctrl Pts',(59.49032073321,-1.49286506234389,339.686207098297));
#62270=CARTESIAN_POINT('Ctrl Pts',(59.482908929033,-1.36859312136543,339.725795881939));
#62271=CARTESIAN_POINT('Ctrl Pts',(59.475497124856,-1.2429024297093,339.760387980409));
#62272=CARTESIAN_POINT('Ctrl Pts',(59.4680853206789,-1.11623072592643,339.789907309019));
#62273=CARTESIAN_POINT('Ctrl Pts',(59.4603102419005,-0.983350464604767,
339.820873467859));
#62274=CARTESIAN_POINT('Ctrl Pts',(59.4525351631221,-0.848970668802507,
339.846354879191));
#62275=CARTESIAN_POINT('Ctrl Pts',(59.4447600843437,-0.713583819411007,
339.866208092054));
#62276=CARTESIAN_POINT('Ctrl Pts',(59.4369945732947,-0.578363572156741,
339.886036874275));
#62277=CARTESIAN_POINT('Ctrl Pts',(59.4292290622456,-0.442139120093809,
339.900251182325));
#62278=CARTESIAN_POINT('Ctrl Pts',(59.4214635511966,-0.305415952404884,
339.908757903841));
#62279=CARTESIAN_POINT('Ctrl Pts',(59.4137057396744,-0.168828346134968,
339.917256190917));
#62280=CARTESIAN_POINT('Ctrl Pts',(59.4059479281523,-0.0317433958850884,
339.920058129249));
#62281=CARTESIAN_POINT('Ctrl Pts',(59.3981901166301,0.105325767257696,339.917122079555));
#62282=CARTESIAN_POINT('Ctrl Pts',(59.3904381431071,0.242291781508595,339.914188239332));
#62283=CARTESIAN_POINT('Ctrl Pts',(59.3826861695841,0.379241643088397,339.905525014224));
#62284=CARTESIAN_POINT('Ctrl Pts',(59.3749341960611,0.515660036810762,339.89114278967));
#62285=CARTESIAN_POINT('Ctrl Pts',(59.3671855055035,0.652020657262393,339.876766655996));
#62286=CARTESIAN_POINT('Ctrl Pts',(59.3594368149458,0.787849869607818,339.856676380959));
#62287=CARTESIAN_POINT('Ctrl Pts',(59.3516881243882,0.922635521961498,339.830934356428));
#62288=CARTESIAN_POINT('Ctrl Pts',(59.3439410460104,1.05739313103445,339.80519768774));
#62289=CARTESIAN_POINT('Ctrl Pts',(59.3361939676326,1.19110722829154,339.773811681772));
#62290=CARTESIAN_POINT('Ctrl Pts',(59.3284468892547,1.32327431633506,339.73689013449));
#62291=CARTESIAN_POINT('Ctrl Pts',(59.3206997459489,1.45544251206599,339.699968277769));
#62292=CARTESIAN_POINT('Ctrl Pts',(59.3129526026431,1.58606329626199,339.657510892365));
#62293=CARTESIAN_POINT('Ctrl Pts',(59.3052054593373,1.71464721869942,339.609681982296));
#62294=CARTESIAN_POINT('Ctrl Pts',(59.2974565743092,1.84326004953243,339.561842319273));
#62295=CARTESIAN_POINT('Ctrl Pts',(59.2897076892811,1.96983474109831,339.508628864775));
#62296=CARTESIAN_POINT('Ctrl Pts',(59.281958804253,2.09390112110671,339.450254055391));
#62297=CARTESIAN_POINT('Ctrl Pts',(59.2742016944783,2.21809918645279,339.391817286382));
#62298=CARTESIAN_POINT('Ctrl Pts',(59.2664445847036,2.3397832677126,339.328208385713));
#62299=CARTESIAN_POINT('Ctrl Pts',(59.2586874749288,2.45850665535286,339.259686383771));
#62300=CARTESIAN_POINT('Ctrl Pts',(59.2509262200027,2.57729348497537,339.191127765863));
#62301=CARTESIAN_POINT('Ctrl Pts',(59.2431649650766,2.6931161386087,339.117651024608));
#62302=CARTESIAN_POINT('Ctrl Pts',(59.2354037101504,2.80555713905839,339.039558416706));
#62303=CARTESIAN_POINT('Ctrl Pts',(59.2276300397458,2.91817800846444,338.961340886081));
#62304=CARTESIAN_POINT('Ctrl Pts',(59.2198563693411,3.02740610322768,338.878492969962));
#62305=CARTESIAN_POINT('Ctrl Pts',(59.2120826989365,3.13285657898505,338.791357635203));
#62306=CARTESIAN_POINT('Ctrl Pts',(59.2046708947593,3.23339830972656,338.70827847124));
#62307=CARTESIAN_POINT('Ctrl Pts',(59.1972590905822,3.33050598870649,338.621302256508));
#62308=CARTESIAN_POINT('Ctrl Pts',(59.1898472864051,3.42387874924105,338.530755920904));
#62309=CARTESIAN_POINT('Ctrl Pts',(59.1820722076266,3.52182798691203,338.435771639668));
#62310=CARTESIAN_POINT('Ctrl Pts',(59.1742971288482,3.61597646754352,338.336558256306));
#62311=CARTESIAN_POINT('Ctrl Pts',(59.1665220500698,3.70593705049126,338.233452278958));
#62312=CARTESIAN_POINT('Ctrl Pts',(59.1587565390208,3.79578693121451,338.130473180079));
#62313=CARTESIAN_POINT('Ctrl Pts',(59.1509910279717,3.88145891367139,338.023611309821));
#62314=CARTESIAN_POINT('Ctrl Pts',(59.1432255169227,3.962601148487,337.913241356378));
#62315=CARTESIAN_POINT('Ctrl Pts',(59.1354677054005,4.04366293054049,337.802980835065));
#62316=CARTESIAN_POINT('Ctrl Pts',(59.1277098938783,4.12020367277377,337.689219465427));
#62317=CARTESIAN_POINT('Ctrl Pts',(59.1199520823561,4.19191067515202,337.572366216939));
#62318=CARTESIAN_POINT('Ctrl Pts',(59.1122001088331,4.26356371573701,337.455600904225));
#62319=CARTESIAN_POINT('Ctrl Pts',(59.1044481353101,4.33039005320381,337.335748675723));
#62320=CARTESIAN_POINT('Ctrl Pts',(59.0966961617871,4.39211955427367,337.213248491125));
#62321=CARTESIAN_POINT('Ctrl Pts',(59.0889474712295,4.45382291286317,337.090800185428));
#62322=CARTESIAN_POINT('Ctrl Pts',(59.0811987806718,4.51043355265627,336.965706502375));
#62323=CARTESIAN_POINT('Ctrl Pts',(59.0734500901142,4.56172678553355,336.838431885234));
#62324=CARTESIAN_POINT('Ctrl Pts',(59.0657030117364,4.61300934642532,336.71118374864));
#62325=CARTESIAN_POINT('Ctrl Pts',(59.0579559333585,4.65897655495544,336.581755942834));
#62326=CARTESIAN_POINT('Ctrl Pts',(59.0502088549807,4.69945163324512,336.450633451045));
#62327=CARTESIAN_POINT('Ctrl Pts',(59.0424617116749,4.73992705075491,336.319509860323));
#62328=CARTESIAN_POINT('Ctrl Pts',(59.0347145683691,4.77491013092729,336.186691928773));
#62329=CARTESIAN_POINT('Ctrl Pts',(59.0269674250633,4.80427391864021,336.052679997518));
#62330=CARTESIAN_POINT('Ctrl Pts',(59.0192185400352,4.83364430795601,335.918637937534));
#62331=CARTESIAN_POINT('Ctrl Pts',(59.0114696550071,4.85739280726976,335.783401725428));
#62332=CARTESIAN_POINT('Ctrl Pts',(59.003720769979,4.87544362183722,335.647481700735));
#62333=CARTESIAN_POINT('Ctrl Pts',(58.9959636602043,4.89351359572576,335.511417409124));
#62334=CARTESIAN_POINT('Ctrl Pts',(58.9882065504296,4.9058737527173,335.374668243146));
#62335=CARTESIAN_POINT('Ctrl Pts',(58.9804494406548,4.91250017683042,335.237750026585));
#62336=CARTESIAN_POINT('Ctrl Pts',(58.9726881857287,4.9191301418927,335.100758645306));
#62337=CARTESIAN_POINT('Ctrl Pts',(58.9649269308025,4.92002026639768,334.963598424111));
#62338=CARTESIAN_POINT('Ctrl Pts',(58.9571656758764,4.91519880358639,334.82678399692));
#62339=CARTESIAN_POINT('Ctrl Pts',(58.9493920054717,4.9103696280059,334.689750711234));
#62340=CARTESIAN_POINT('Ctrl Pts',(58.941618335067,4.8998106374413,334.553064714843));
#62341=CARTESIAN_POINT('Ctrl Pts',(58.9338446646624,4.88360197867112,334.417235230629));
#62342=CARTESIAN_POINT('Ctrl Pts',(58.9264328604853,4.86814783686622,334.287728641584));
#62343=CARTESIAN_POINT('Ctrl Pts',(58.9190210563082,4.84755821947558,334.159000902143));
#62344=CARTESIAN_POINT('Ctrl Pts',(58.9116092521311,4.82194523259748,334.031481938046));
#62345=CARTESIAN_POINT('Ctrl Pts',(58.9038341733526,4.79507687693537,333.89771288966));
#62346=CARTESIAN_POINT('Ctrl Pts',(58.8960590945742,4.76259537134975,333.764851369127));
#62347=CARTESIAN_POINT('Ctrl Pts',(58.8882840157958,4.7245741886985,333.633405035139));
#62348=CARTESIAN_POINT('Ctrl Pts',(58.8805185047467,4.68659979353305,333.502120454233));
#62349=CARTESIAN_POINT('Ctrl Pts',(58.8727529936978,4.64309939259957,333.372247966724));
#62350=CARTESIAN_POINT('Ctrl Pts',(58.8649874826488,4.59419766330899,333.244286215539));
#62351=CARTESIAN_POINT('Ctrl Pts',(58.8572296711266,4.54534442022537,333.116451338803));
#62352=CARTESIAN_POINT('Ctrl Pts',(58.8494718596044,4.49110064503393,332.990523790997));
#62353=CARTESIAN_POINT('Ctrl Pts',(58.8417140480822,4.4316410289586,332.8669878451));
#62354=CARTESIAN_POINT('Ctrl Pts',(58.8339620745592,4.37222615812998,332.74354486392));
#62355=CARTESIAN_POINT('Ctrl Pts',(58.8262101010361,4.30760342794561,332.622490253105));
#62356=CARTESIAN_POINT('Ctrl Pts',(58.8184581275131,4.23799578435709,332.504288719769));
#62357=CARTESIAN_POINT('Ctrl Pts',(58.8107094369555,4.16841761964691,332.386137244853));
#62358=CARTESIAN_POINT('Ctrl Pts',(58.8029607463979,4.09385893832118,332.270836780342));
#62359=CARTESIAN_POINT('Ctrl Pts',(58.7952120558402,4.0145887089974,332.158827608171));
#62360=CARTESIAN_POINT('Ctrl Pts',(58.7874649774624,3.93533497250691,332.046841740444));
#62361=CARTESIAN_POINT('Ctrl Pts',(58.7797178990845,3.8513718635168,331.938146121836));
#62362=CARTESIAN_POINT('Ctrl Pts',(58.7719708207067,3.76301155011732,331.83315186089));
#62363=CARTESIAN_POINT('Ctrl Pts',(58.7642236774009,3.67465049617336,331.728156719991));
#62364=CARTESIAN_POINT('Ctrl Pts',(58.7564765340951,3.58189241599727,331.62686329769));
#62365=CARTESIAN_POINT('Ctrl Pts',(58.7487293907893,3.48508935441027,331.529649116548));
#62366=CARTESIAN_POINT('Ctrl Pts',(58.7409805057612,3.38826452943997,331.432413079594));
#62367=CARTESIAN_POINT('Ctrl Pts',(58.7332316207331,3.28739318920863,331.339258385646));
#62368=CARTESIAN_POINT('Ctrl Pts',(58.725482735705,3.18286347223618,331.250524946129));
#62369=CARTESIAN_POINT('Ctrl Pts',(58.7177256259303,3.07822280634199,331.161697324021));
#62370=CARTESIAN_POINT('Ctrl Pts',(58.7099685161556,2.96991630542968,331.077300583939));
#62371=CARTESIAN_POINT('Ctrl Pts',(58.7022114063809,2.85836479441284,330.997633979187));
#62372=CARTESIAN_POINT('Ctrl Pts',(58.6944501514547,2.74675367383532,330.917924803148));
#62373=CARTESIAN_POINT('Ctrl Pts',(58.6866888965286,2.6318944150919,330.842951012521));
#62374=CARTESIAN_POINT('Ctrl Pts',(58.6789276416024,2.51423507427683,330.772967346498));
#62375=CARTESIAN_POINT('Ctrl Pts',(58.6711539711977,2.39638751686146,330.702871729416));
#62376=CARTESIAN_POINT('Ctrl Pts',(58.663380300793,2.27573127075965,330.63778237416));
#62377=CARTESIAN_POINT('Ctrl Pts',(58.6556066303884,2.15273792437585,330.577907453314));
#62378=CARTESIAN_POINT('Ctrl Pts',(58.6481948262113,2.03546994785687,330.520819724439));
#62379=CARTESIAN_POINT('Ctrl Pts',(58.6407830220342,1.9160778220735,330.468472006755));
#62380=CARTESIAN_POINT('Ctrl Pts',(58.6333712178572,1.7949837477944,330.421002685341));
#62381=CARTESIAN_POINT('Ctrl Pts',(58.6255961390787,1.66795449221406,330.37120675108));
#62382=CARTESIAN_POINT('Ctrl Pts',(58.6178210603003,1.53865079866103,330.326622149737));
#62383=CARTESIAN_POINT('Ctrl Pts',(58.6100459815219,1.40753932853812,330.287461819665));
#62384=CARTESIAN_POINT('Ctrl Pts',(58.6022804704729,1.27658919942616,330.248349678872));
#62385=CARTESIAN_POINT('Ctrl Pts',(58.5945149594238,1.14383609097412,330.214648638984));
#62386=CARTESIAN_POINT('Ctrl Pts',(58.5867494483748,1.00976679275898,330.186523700407));
#62387=CARTESIAN_POINT('Ctrl Pts',(58.5789916368526,0.875830424643447,330.158426647789));
#62388=CARTESIAN_POINT('Ctrl Pts',(58.5712338253304,0.740580843883713,330.135894773749));
#62389=CARTESIAN_POINT('Ctrl Pts',(58.5634760138082,0.604519821404695,330.119043244606));
#62390=CARTESIAN_POINT('Ctrl Pts',(58.5557240402852,0.468561189159927,330.102204396773));
#62391=CARTESIAN_POINT('Ctrl Pts',(58.5479720667622,0.331792716984758,330.091037433226));
#62392=CARTESIAN_POINT('Ctrl Pts',(58.5402200932392,0.194725835852015,330.085606353643));
#62393=CARTESIAN_POINT('Ctrl Pts',(58.5324714026816,0.057717002624715,330.080177574126));
#62394=CARTESIAN_POINT('Ctrl Pts',(58.524722712124,-0.0795895984514916,
330.080479862606));
#62395=CARTESIAN_POINT('Ctrl Pts',(58.5169740215664,-0.216678170552494,
330.086525299454));
#62396=CARTESIAN_POINT('Ctrl Pts',(58.5092269431886,-0.353738220231084,
330.092569478498));
#62397=CARTESIAN_POINT('Ctrl Pts',(58.5014798648107,-0.490579940914575,
330.10435441194));
#62398=CARTESIAN_POINT('Ctrl Pts',(58.4937327864329,-0.626688690592526,
330.121840065395));
#62399=CARTESIAN_POINT('Ctrl Pts',(58.4859856431271,-0.762798580992895,
330.139325865397));
#62400=CARTESIAN_POINT('Ctrl Pts',(58.4782384998213,-0.89817510044688,330.162512430901));
#62401=CARTESIAN_POINT('Ctrl Pts',(58.4704913565155,-1.03231027052626,330.191308019028));
#62402=CARTESIAN_POINT('Ctrl Pts',(58.4627424714874,-1.16647559703955,330.220110081014));
#62403=CARTESIAN_POINT('Ctrl Pts',(58.4549935864593,-1.29939863674428,330.2545235929));
#62404=CARTESIAN_POINT('Ctrl Pts',(58.4472447014312,-1.43058350684719,330.294406106299));
#62405=CARTESIAN_POINT('Ctrl Pts',(58.4394875916564,-1.56190761792671,330.33433095141));
#62406=CARTESIAN_POINT('Ctrl Pts',(58.4317304818817,-1.69148949945696,330.379736279902));
#62407=CARTESIAN_POINT('Ctrl Pts',(58.423973372107,-1.8188497704412,330.430430154263));
#62408=CARTESIAN_POINT('Ctrl Pts',(58.4162121171808,-1.94627809868206,330.48115111781));
#62409=CARTESIAN_POINT('Ctrl Pts',(58.4084508622546,-2.071482094245,330.537166098798));
#62410=CARTESIAN_POINT('Ctrl Pts',(58.4006896073285,-2.19400507264695,330.598236171295));
#62411=CARTESIAN_POINT('Ctrl Pts',(58.3929159369238,-2.31672404788412,330.659403936004));
#62412=CARTESIAN_POINT('Ctrl Pts',(58.3851422665192,-2.43675309335869,330.725642762484));
#62413=CARTESIAN_POINT('Ctrl Pts',(58.3773685961145,-2.5536619487584,330.796668736114));
#62414=CARTESIAN_POINT('Ctrl Pts',(58.3699567919374,-2.66512866881277,330.864388433584));
#62415=CARTESIAN_POINT('Ctrl Pts',(58.3625449877603,-2.77375891138264,330.936459465524));
#62416=CARTESIAN_POINT('Ctrl Pts',(58.3551331835832,-2.87920782844273,331.012601682408));
#62417=CARTESIAN_POINT('Ctrl Pts',(58.3474209354891,-2.98893120890391,331.091830390158));
#62418=CARTESIAN_POINT('Ctrl Pts',(58.3397086873949,-3.09556902993061,331.175726748648));
#62419=CARTESIAN_POINT('Ctrl Pts',(58.3319964393008,-3.19869354984864,331.264020525129));
#62420=CARTESIAN_POINT('Ctrl Pts',(58.3242937129603,-3.30169074939654,331.352205291684));
#62421=CARTESIAN_POINT('Ctrl Pts',(58.3165909866199,-3.40118297654752,331.444776421024));
#62422=CARTESIAN_POINT('Ctrl Pts',(58.3088882602795,-3.49677157664729,331.541420580173));
#62423=CARTESIAN_POINT('Ctrl Pts',(58.3011931263538,-3.59226595708197,331.637969479215));
#62424=CARTESIAN_POINT('Ctrl Pts',(58.2934979924281,-3.68386408741934,331.738583139987));
#62425=CARTESIAN_POINT('Ctrl Pts',(58.2858028585024,-3.77120087739879,331.842908457962));
#62426=CARTESIAN_POINT('Ctrl Pts',(58.2777201300872,-3.86293671473137,331.952488514679));
#62427=CARTESIAN_POINT('Ctrl Pts',(58.269637401672,-3.94997042934416,332.066163570637));
#62428=CARTESIAN_POINT('Ctrl Pts',(58.2615546732568,-4.03192290163398,332.18348073364));
#62429=CARTESIAN_POINT('Ctrl Pts',(58.2538683894613,-4.10985573908783,332.295043681521));
#62430=CARTESIAN_POINT('Ctrl Pts',(58.2461821056658,-4.18319365383043,332.409899603287));
#62431=CARTESIAN_POINT('Ctrl Pts',(58.2384958218702,-4.25165263303496,332.527626049622));
#62432=CARTESIAN_POINT('Ctrl Pts',(58.2308108083021,-4.32010029877827,332.645333040605));
#62433=CARTESIAN_POINT('Ctrl Pts',(58.223125794734,-4.38367043255201,332.765909268929));
#62434=CARTESIAN_POINT('Ctrl Pts',(58.2154407811659,-4.44212360917944,332.888905283207));
#62435=CARTESIAN_POINT('Ctrl Pts',(58.2077553068613,-4.50058029022692,333.011908671416));
#62436=CARTESIAN_POINT('Ctrl Pts',(58.2000698325566,-4.55391923342674,333.137331774642));
#62437=CARTESIAN_POINT('Ctrl Pts',(58.1923843582519,-4.60194825193857,333.264703094863));
#62438=CARTESIAN_POINT('Ctrl Pts',(58.1846966922218,-4.64999096725272,333.392110738537));
#62439=CARTESIAN_POINT('Ctrl Pts',(58.1770090261917,-4.6927206059285,333.52146733209));
#62440=CARTESIAN_POINT('Ctrl Pts',(58.1693213601616,-4.72999430503115,333.652284548997));
#62441=CARTESIAN_POINT('Ctrl Pts',(58.161625698353,-4.76730677171792,333.783237826117));
#62442=CARTESIAN_POINT('Ctrl Pts',(58.1539300365445,-4.79915186202804,333.915654376344));
#62443=CARTESIAN_POINT('Ctrl Pts',(58.1462343747359,-4.82543739887673,334.049033664096));
#62444=CARTESIAN_POINT('Ctrl Pts',(58.1385340507997,-4.85173885983083,334.182493754682));
#62445=CARTESIAN_POINT('Ctrl Pts',(58.1308337268634,-4.87247400025397,334.316917351973));
#62446=CARTESIAN_POINT('Ctrl Pts',(58.1231334029271,-4.88760246885154,334.45179824063));
#62447=CARTESIAN_POINT('Ctrl Pts',(58.1154224216085,-4.90275187551296,334.586865806785));
#62448=CARTESIAN_POINT('Ctrl Pts',(58.1077114402899,-4.9122790939977,334.722391532249));
#62449=CARTESIAN_POINT('Ctrl Pts',(58.1000004589713,-4.91619585075647,334.857868302251));
#62450=CARTESIAN_POINT('Ctrl Pts',(58.0972727648267,-4.91758137019104,334.905792058903));
#62451=CARTESIAN_POINT('Ctrl Pts',(58.0945450706822,-4.91826531006321,334.953709729097));
#62452=CARTESIAN_POINT('Ctrl Pts',(58.0918173765376,-4.9182497400553,335.001599045328));
#62453=CARTESIAN_POINT('',(56.3418173765458,-4.91824791469108,334.995470967337));
#62454=CARTESIAN_POINT('Ctrl Pts',(58.0918173765087,-4.91824974005514,335.001599045835));
#62455=CARTESIAN_POINT('Ctrl Pts',(58.0868433007755,-4.91822134742056,335.088927416654));
#62456=CARTESIAN_POINT('Ctrl Pts',(58.0818692250423,-4.91586720613331,335.176215108472));
#62457=CARTESIAN_POINT('Ctrl Pts',(58.0768951493091,-4.91119287755596,335.26337726163));
#62458=CARTESIAN_POINT('Ctrl Pts',(58.0691200705307,-4.90388633964328,335.39962219308));
#62459=CARTESIAN_POINT('Ctrl Pts',(58.0613449917522,-4.89089445730422,335.535778143507));
#62460=CARTESIAN_POINT('Ctrl Pts',(58.0535699129738,-4.87221676308775,335.671332165166));
#62461=CARTESIAN_POINT('Ctrl Pts',(58.0458044019248,-4.85356205296308,335.806719378972));
#62462=CARTESIAN_POINT('Ctrl Pts',(58.0380388908758,-4.82923550533785,335.941505754299));
#62463=CARTESIAN_POINT('Ctrl Pts',(58.0302733798268,-4.79928862213002,336.075179884481));
#62464=CARTESIAN_POINT('Ctrl Pts',(58.0225155683046,-4.76937143134412,336.208721476374));
#62465=CARTESIAN_POINT('Ctrl Pts',(58.0147577567824,-4.73384507962182,336.341152638782));
#62466=CARTESIAN_POINT('Ctrl Pts',(58.0069999452602,-4.69281263168756,336.471968976023));
#62467=CARTESIAN_POINT('Ctrl Pts',(57.9992479717372,-4.65181106197162,336.602686869821));
#62468=CARTESIAN_POINT('Ctrl Pts',(57.9914959982142,-4.60531176001444,336.731791985806));
#62469=CARTESIAN_POINT('Ctrl Pts',(57.9837440246912,-4.55346836156164,336.85879233449));
#62470=CARTESIAN_POINT('Ctrl Pts',(57.9759953341336,-4.5016469188188,336.98573889845));
#62471=CARTESIAN_POINT('Ctrl Pts',(57.9682466435759,-4.44448602840014,337.110582106852));
#62472=CARTESIAN_POINT('Ctrl Pts',(57.9604979530183,-4.38218838873212,337.232847506697));
#62473=CARTESIAN_POINT('Ctrl Pts',(57.9527508746405,-4.31990371060835,337.355087468204));
#62474=CARTESIAN_POINT('Ctrl Pts',(57.9450037962627,-4.25248458638428,337.474750339909));
#62475=CARTESIAN_POINT('Ctrl Pts',(57.9372567178848,-4.18018066785445,337.591384310865));
#62476=CARTESIAN_POINT('Ctrl Pts',(57.929509574579,-4.10787614334819,337.708019259325));
#62477=CARTESIAN_POINT('Ctrl Pts',(57.9217624312732,-4.03068694882805,337.821624924187));
#62478=CARTESIAN_POINT('Ctrl Pts',(57.9140152879674,-3.94890703743601,337.931776982001));
#62479=CARTESIAN_POINT('Ctrl Pts',(57.9062664029393,-3.86710874018376,338.041953804335));
#62480=CARTESIAN_POINT('Ctrl Pts',(57.8985175179112,-3.78071790526986,338.148675160808));
#62481=CARTESIAN_POINT('Ctrl Pts',(57.8907686328831,-3.69006962383433,338.251548743869));
#62482=CARTESIAN_POINT('Ctrl Pts',(57.8830115231084,-3.59932512737618,338.354531518014));
#62483=CARTESIAN_POINT('Ctrl Pts',(57.8752544133336,-3.50431441629685,338.453658066711));
#62484=CARTESIAN_POINT('Ctrl Pts',(57.8674973035589,-3.40541078719704,338.548571604596));
#62485=CARTESIAN_POINT('Ctrl Pts',(57.8597360486327,-3.30645430716023,338.64353586124));
#62486=CARTESIAN_POINT('Ctrl Pts',(57.8519747937065,-3.20360105696828,338.734282362688));
#62487=CARTESIAN_POINT('Ctrl Pts',(57.8442135387804,-3.09725769623202,338.820494447795));
#62488=CARTESIAN_POINT('Ctrl Pts',(57.8364398683757,-2.99074422077581,338.906844444141));
#62489=CARTESIAN_POINT('Ctrl Pts',(57.8286661979711,-2.88072979204245,338.98864529598));
#62490=CARTESIAN_POINT('Ctrl Pts',(57.8208925275664,-2.76765106825078,339.065623030596));
#62491=CARTESIAN_POINT('Ctrl Pts',(57.8134807233894,-2.65983618625762,339.139017433145));
#62492=CARTESIAN_POINT('Ctrl Pts',(57.8060689192124,-2.54923611906024,339.208027493147));
#62493=CARTESIAN_POINT('Ctrl Pts',(57.7986571150353,-2.43624871202379,339.272455415293));
#62494=CARTESIAN_POINT('Ctrl Pts',(57.7908820362569,-2.31772345559552,339.340041141824));
#62495=CARTESIAN_POINT('Ctrl Pts',(57.7831069574784,-2.19619635911406,339.402797788198));
#62496=CARTESIAN_POINT('Ctrl Pts',(57.7753318787,-2.07209851831654,339.460447375868));
#62497=CARTESIAN_POINT('Ctrl Pts',(57.767566367651,-1.94815338781258,339.518026022051));
#62498=CARTESIAN_POINT('Ctrl Pts',(57.759800856602,-1.82164415848191,339.570509950898));
#62499=CARTESIAN_POINT('Ctrl Pts',(57.752035345553,-1.69302875374377,339.617665719982));
#62500=CARTESIAN_POINT('Ctrl Pts',(57.7442775340308,-1.56454087155396,339.664774733983));
#62501=CARTESIAN_POINT('Ctrl Pts',(57.7365197225086,-1.43395133437161,339.706565967776));
#62502=CARTESIAN_POINT('Ctrl Pts',(57.7287619109864,-1.30174007352346,339.74285313324));
#62503=CARTESIAN_POINT('Ctrl Pts',(57.7210099374634,-1.16962830584176,339.779112991461));
#62504=CARTESIAN_POINT('Ctrl Pts',(57.7132579639404,-1.03589761905483,339.809876922736));
#62505=CARTESIAN_POINT('Ctrl Pts',(57.7055059904174,-0.901044878736802,
339.835007878898));
#62506=CARTESIAN_POINT('Ctrl Pts',(57.6977572998598,-0.766249248634269,
339.860128192085));
#62507=CARTESIAN_POINT('Ctrl Pts',(57.6900086093022,-0.630332893579719,
339.879620203426));
#62508=CARTESIAN_POINT('Ctrl Pts',(57.6822599187446,-0.493804482970295,
339.89339761261));
#62509=CARTESIAN_POINT('Ctrl Pts',(57.6745128403667,-0.357304478237098,
339.90717215529));
#62510=CARTESIAN_POINT('Ctrl Pts',(57.6667657619889,-0.220193059898798,
339.91523442154));
#62511=CARTESIAN_POINT('Ctrl Pts',(57.6590186836111,-0.0829852663312264,
339.917549848052));
#62512=CARTESIAN_POINT('Ctrl Pts',(57.6512715403053,0.0542236771699033,
339.919865293969));
#62513=CARTESIAN_POINT('Ctrl Pts',(57.6435243969995,0.19152860669271,339.916433797486));
#62514=CARTESIAN_POINT('Ctrl Pts',(57.6357772536937,0.328413624683528,339.907272924306));
#62515=CARTESIAN_POINT('Ctrl Pts',(57.6280283686656,0.465329417332357,339.898109991566));
#62516=CARTESIAN_POINT('Ctrl Pts',(57.6202794836375,0.601824720668057,339.883215145077));
#62517=CARTESIAN_POINT('Ctrl Pts',(57.6125305986095,0.737388297857424,339.862657870001));
#62518=CARTESIAN_POINT('Ctrl Pts',(57.6047734888347,0.873095763628347,339.842078775221));
#62519=CARTESIAN_POINT('Ctrl Pts',(57.59701637906,1.00786914067846,339.81582530469));
#62520=CARTESIAN_POINT('Ctrl Pts',(57.5892592692853,1.14120638837211,339.784018294451));
#62521=CARTESIAN_POINT('Ctrl Pts',(57.5814980143591,1.27461488722762,339.752194287562));
#62522=CARTESIAN_POINT('Ctrl Pts',(57.5737367594329,1.40658535168398,339.714810934165));
#62523=CARTESIAN_POINT('Ctrl Pts',(57.5659755045068,1.53663142777966,339.672038839485));
#62524=CARTESIAN_POINT('Ctrl Pts',(57.5582018341021,1.66688553521517,339.629198323394));
#62525=CARTESIAN_POINT('Ctrl Pts',(57.5504281636975,1.79520873668472,339.580951977879));
#62526=CARTESIAN_POINT('Ctrl Pts',(57.5426544932928,1.92113434187087,339.527518735796));
#62527=CARTESIAN_POINT('Ctrl Pts',(57.5352426891157,2.04119807984042,339.476572823987));
#62528=CARTESIAN_POINT('Ctrl Pts',(57.5278308849385,2.15908215415359,339.420912171195));
#62529=CARTESIAN_POINT('Ctrl Pts',(57.5204190807614,2.27440493756041,339.360764295683));
#62530=CARTESIAN_POINT('Ctrl Pts',(57.512644001983,2.39538003411008,339.297668393621));
#62531=CARTESIAN_POINT('Ctrl Pts',(57.5048689232046,2.51391872203002,339.229434887852));
#62532=CARTESIAN_POINT('Ctrl Pts',(57.4970938444261,2.62955395258996,339.156275865835));
#62533=CARTESIAN_POINT('Ctrl Pts',(57.4893283333771,2.74504688663707,339.083206870652));
#62534=CARTESIAN_POINT('Ctrl Pts',(57.4815628223281,2.85764314518981,339.005224626178));
#62535=CARTESIAN_POINT('Ctrl Pts',(57.4737973112791,2.96689861289058,338.922587880893));
#62536=CARTESIAN_POINT('Ctrl Pts',(57.4660394997569,3.07604575347703,338.840033070181));
#62537=CARTESIAN_POINT('Ctrl Pts',(57.4582816882347,3.18185838534588,338.752833176945));
#62538=CARTESIAN_POINT('Ctrl Pts',(57.4505238767125,3.28392013646286,338.661290974483));
#62539=CARTESIAN_POINT('Ctrl Pts',(57.4427719031895,3.38590508287556,338.569817660433));
#62540=CARTESIAN_POINT('Ctrl Pts',(57.4350199296665,3.48414447708982,338.474008801341));
#62541=CARTESIAN_POINT('Ctrl Pts',(57.4272679561435,3.57825418990664,338.374208057443));
#62542=CARTESIAN_POINT('Ctrl Pts',(57.4195192655859,3.67232404720414,338.27444957922));
#62543=CARTESIAN_POINT('Ctrl Pts',(57.4117705750282,3.76226743398327,338.170702862394));
#62544=CARTESIAN_POINT('Ctrl Pts',(57.4040218844706,3.847736508274,338.063348955864));
#62545=CARTESIAN_POINT('Ctrl Pts',(57.3962748060928,3.93318780000991,337.956017385211));
#62546=CARTESIAN_POINT('Ctrl Pts',(57.388527727715,4.0141663876148,337.845080423267));
#62547=CARTESIAN_POINT('Ctrl Pts',(57.3807806493371,4.09036448924706,337.730952472601));
#62548=CARTESIAN_POINT('Ctrl Pts',(57.3730335060313,4.16656322949281,337.616823565433));
#62549=CARTESIAN_POINT('Ctrl Pts',(57.3652863627255,4.2379811868127,337.499503941279));
#62550=CARTESIAN_POINT('Ctrl Pts',(57.3575392194197,4.30435395081173,337.379436935208));
#62551=CARTESIAN_POINT('Ctrl Pts',(57.3497903343917,4.37074163681724,337.259342935525));
#62552=CARTESIAN_POINT('Ctrl Pts',(57.3420414493635,4.43208168337109,337.136500666849));
#62553=CARTESIAN_POINT('Ctrl Pts',(57.3342925643354,4.48815586244286,337.011377641548));
#62554=CARTESIAN_POINT('Ctrl Pts',(57.3265354545607,4.54428955922765,336.886121809376));
#62555=CARTESIAN_POINT('Ctrl Pts',(57.318778344786,4.59514606338159,336.758580742022));
#62556=CARTESIAN_POINT('Ctrl Pts',(57.3110212350113,4.64055530551533,336.629242007485));
#62557=CARTESIAN_POINT('Ctrl Pts',(57.3032599800851,4.68598881289616,336.499834158463));
#62558=CARTESIAN_POINT('Ctrl Pts',(57.2954987251589,4.72596914426627,336.368627101856));
#62559=CARTESIAN_POINT('Ctrl Pts',(57.2877374702328,4.76037657116539,336.236122147362));
#62560=CARTESIAN_POINT('Ctrl Pts',(57.2799637998281,4.7948390387342,336.103405228125));
#62561=CARTESIAN_POINT('Ctrl Pts',(57.2721901294235,4.82371070499877,335.969386644421));
#62562=CARTESIAN_POINT('Ctrl Pts',(57.2644164590188,4.84692312235904,335.834577323225));
#62563=CARTESIAN_POINT('Ctrl Pts',(57.2570046548417,4.86905499610667,335.706043408364));
#62564=CARTESIAN_POINT('Ctrl Pts',(57.2495928506646,4.88604260250294,335.576791002294));
#62565=CARTESIAN_POINT('Ctrl Pts',(57.2421810464875,4.89787074610759,335.4472641467));
#62566=CARTESIAN_POINT('Ctrl Pts',(57.2344059677091,4.9102786222645,335.311388794073));
#62567=CARTESIAN_POINT('Ctrl Pts',(57.2266308889306,4.91704769734693,335.17478201728));
#62568=CARTESIAN_POINT('Ctrl Pts',(57.2188558101522,4.9181035733576,335.037951340255));
#62569=CARTESIAN_POINT('Ctrl Pts',(57.2110902991032,4.91915815004562,334.90128904209));
#62570=CARTESIAN_POINT('Ctrl Pts',(57.2033247880542,4.91451351326451,334.764403779032));
#62571=CARTESIAN_POINT('Ctrl Pts',(57.1955592770051,4.90414691382683,334.62780904081));
#62572=CARTESIAN_POINT('Ctrl Pts',(57.1878014654829,4.89379059290269,334.491349736669));
#62573=CARTESIAN_POINT('Ctrl Pts',(57.1800436539608,4.87772362898367,334.355180771358));
#62574=CARTESIAN_POINT('Ctrl Pts',(57.1722858424386,4.85597530779821,334.219816129009));
#62575=CARTESIAN_POINT('Ctrl Pts',(57.1645338689155,4.83424335291412,334.084553352847));
#62576=CARTESIAN_POINT('Ctrl Pts',(57.1567818953925,4.80683861249617,333.950094079241));
#62577=CARTESIAN_POINT('Ctrl Pts',(57.1490299218695,4.77384220341668,333.816947304902));
#62578=CARTESIAN_POINT('Ctrl Pts',(57.1412812313119,4.74085976833602,333.683856918302));
#62579=CARTESIAN_POINT('Ctrl Pts',(57.1335325407543,4.70229046835472,333.552078304041));
#62580=CARTESIAN_POINT('Ctrl Pts',(57.1257838501967,4.6582664983716,333.422110177278));
#62581=CARTESIAN_POINT('Ctrl Pts',(57.1180367718188,4.61425168794314,333.29216909147));
#62582=CARTESIAN_POINT('Ctrl Pts',(57.110289693441,4.56478459021156,333.164038113881));
#62583=CARTESIAN_POINT('Ctrl Pts',(57.1025426150632,4.51004712672267,333.038200321837));
#62584=CARTESIAN_POINT('Ctrl Pts',(57.0947954717574,4.45530920448116,332.912361475151));
#62585=CARTESIAN_POINT('Ctrl Pts',(57.0870483284516,4.39530098429308,332.788816210778));
#62586=CARTESIAN_POINT('Ctrl Pts',(57.0793011851458,4.33025218843889,332.668026791102));
#62587=CARTESIAN_POINT('Ctrl Pts',(57.0715523001177,4.26518876823442,332.5472102154));
#62588=CARTESIAN_POINT('Ctrl Pts',(57.0638034150896,4.19508270266151,332.429151061352));
#62589=CARTESIAN_POINT('Ctrl Pts',(57.0560545300615,4.12020903713502,332.314285839332));
#62590=CARTESIAN_POINT('Ctrl Pts',(57.0482974202868,4.04525589992625,332.199298698179));
#62591=CARTESIAN_POINT('Ctrl Pts',(57.0405403105121,3.96552526796268,332.08751258901));
#62592=CARTESIAN_POINT('Ctrl Pts',(57.0327832007373,3.88133511326965,331.979334377823));
#62593=CARTESIAN_POINT('Ctrl Pts',(57.0250219458112,3.7970999700499,331.871098359659));
#62594=CARTESIAN_POINT('Ctrl Pts',(57.017260690885,3.70840080834417,331.766474379077));
#62595=CARTESIAN_POINT('Ctrl Pts',(57.0094994359588,3.61559439823423,331.665834405739));
#62596=CARTESIAN_POINT('Ctrl Pts',(57.0017257655541,3.52263952811359,331.565033441241));
#62597=CARTESIAN_POINT('Ctrl Pts',(56.9939520951495,3.42556455718725,331.468229495502));
#62598=CARTESIAN_POINT('Ctrl Pts',(56.9861784247448,3.32476209392481,331.375756619472));
#62599=CARTESIAN_POINT('Ctrl Pts',(56.9787666205677,3.22865200957877,331.287588378069));
#62600=CARTESIAN_POINT('Ctrl Pts',(56.9713548163906,3.12915387240548,331.20335724401));
#62601=CARTESIAN_POINT('Ctrl Pts',(56.9639430122135,3.0266328634056,331.123316291899));
#62602=CARTESIAN_POINT('Ctrl Pts',(56.9561679334351,2.91908699436039,331.039352294296));
#62603=CARTESIAN_POINT('Ctrl Pts',(56.9483928546567,2.80787457631343,330.959734269229));
#62604=CARTESIAN_POINT('Ctrl Pts',(56.9406177758782,2.69338213594443,330.884799429885));
#62605=CARTESIAN_POINT('Ctrl Pts',(56.9328522648292,2.57903058581233,330.809956802631));
#62606=CARTESIAN_POINT('Ctrl Pts',(56.9250867537802,2.46140736831671,330.739786106474));
#62607=CARTESIAN_POINT('Ctrl Pts',(56.9173212427312,2.34093197703384,330.674584350447));
#62608=CARTESIAN_POINT('Ctrl Pts',(56.909563431209,2.22057603745219,330.60944724215));
#62609=CARTESIAN_POINT('Ctrl Pts',(56.9018056196868,2.09737389338583,330.54926945438));
#62610=CARTESIAN_POINT('Ctrl Pts',(56.8940478081646,1.97177361324516,330.494304506449));
#62611=CARTESIAN_POINT('Ctrl Pts',(56.8862958346416,1.84626785129832,330.439380921384));
#62612=CARTESIAN_POINT('Ctrl Pts',(56.8785438611186,1.71836790203643,330.389662524036));
#62613=CARTESIAN_POINT('Ctrl Pts',(56.8707918875955,1.5885456886467,330.345356548823));
#62614=CARTESIAN_POINT('Ctrl Pts',(56.8630431970379,1.45877845504142,330.301069337218));
#62615=CARTESIAN_POINT('Ctrl Pts',(56.8552945064803,1.32709094561055,330.26219011478));
#62616=CARTESIAN_POINT('Ctrl Pts',(56.8475458159227,1.19397407881431,330.228877599388));
#62617=CARTESIAN_POINT('Ctrl Pts',(56.8397987375448,1.06088490809403,330.195572014943));
#62618=CARTESIAN_POINT('Ctrl Pts',(56.832051659167,0.926367350480988,330.167830928633));
#62619=CARTESIAN_POINT('Ctrl Pts',(56.8243045807892,0.790926084190972,330.145762779607));
#62620=CARTESIAN_POINT('Ctrl Pts',(56.8165574374834,0.655483682772783,330.123694445629));
#62621=CARTESIAN_POINT('Ctrl Pts',(56.8088102941776,0.519117943023406,330.107299206626));
#62622=CARTESIAN_POINT('Ctrl Pts',(56.8010631508718,0.382341907152689,330.096634040933));
#62623=CARTESIAN_POINT('Ctrl Pts',(56.7933142658437,0.245535121125271,330.085966477484));
#62624=CARTESIAN_POINT('Ctrl Pts',(56.7855653808156,0.108318245037932,330.081031581184));
#62625=CARTESIAN_POINT('Ctrl Pts',(56.7778164957875,-0.0287928073667623,
330.081834281285));
#62626=CARTESIAN_POINT('Ctrl Pts',(56.7700593860127,-0.166049390859194,
330.08263783338));
#62627=CARTESIAN_POINT('Ctrl Pts',(56.762302276238,-0.303199534809589,330.08919114482));
#62628=CARTESIAN_POINT('Ctrl Pts',(56.7545451664633,-0.439729024012318,
330.101447004682));
#62629=CARTESIAN_POINT('Ctrl Pts',(56.7467839115371,-0.576331470208617,
330.113709413683));
#62630=CARTESIAN_POINT('Ctrl Pts',(56.7390226566109,-0.712312213490378,
330.13168039186));
#62631=CARTESIAN_POINT('Ctrl Pts',(56.7312614016848,-0.84716538787191,330.155261217765));
#62632=CARTESIAN_POINT('Ctrl Pts',(56.7234877312801,-0.982234283383906,
330.178879765307));
#62633=CARTESIAN_POINT('Ctrl Pts',(56.7157140608755,-1.11617162350625,330.208126009714));
#62634=CARTESIAN_POINT('Ctrl Pts',(56.7079403904708,-1.24848403469736,330.242850572285));
#62635=CARTESIAN_POINT('Ctrl Pts',(56.7005285862938,-1.37463727131428,330.275958698115));
#62636=CARTESIAN_POINT('Ctrl Pts',(56.6931167821167,-1.49931318016239,330.314046504542));
#62637=CARTESIAN_POINT('Ctrl Pts',(56.6857049779397,-1.62210132501434,330.356943856264));
#62638=CARTESIAN_POINT('Ctrl Pts',(56.6779298991612,-1.75090768261332,330.401943734978));
#62639=CARTESIAN_POINT('Ctrl Pts',(56.6701548203828,-1.87804359924059,330.452378748082));
#62640=CARTESIAN_POINT('Ctrl Pts',(56.6623797416044,-2.00301633336829,330.508106342448));
#62641=CARTESIAN_POINT('Ctrl Pts',(56.6546142305554,-2.12783528059057,330.563765360461));
#62642=CARTESIAN_POINT('Ctrl Pts',(56.6468487195063,-2.25049598822098,330.62470384335));
#62643=CARTESIAN_POINT('Ctrl Pts',(56.6390832084573,-2.37052168298279,330.690729758647));
#62644=CARTESIAN_POINT('Ctrl Pts',(56.6313253969351,-2.4904283719188,330.756690209057));
#62645=CARTESIAN_POINT('Ctrl Pts',(56.6235675854129,-2.60770490698363,330.827727866442));
#62646=CARTESIAN_POINT('Ctrl Pts',(56.6158097738907,-2.72189562285166,330.903603134363));
#62647=CARTESIAN_POINT('Ctrl Pts',(56.6080578003677,-2.8360004065848,330.979421303739));
#62648=CARTESIAN_POINT('Ctrl Pts',(56.6003058268446,-2.94702366905328,331.060069622053));
#62649=CARTESIAN_POINT('Ctrl Pts',(56.5925538533216,-3.05453575769835,331.145263385464));
#62650=CARTESIAN_POINT('Ctrl Pts',(56.584805162764,-3.16200231491004,331.230421069266));
#62651=CARTESIAN_POINT('Ctrl Pts',(56.5770564722064,-3.26596035009034,331.320120127226));
#62652=CARTESIAN_POINT('Ctrl Pts',(56.5693077816487,-3.36601072984262,331.414033626889));
#62653=CARTESIAN_POINT('Ctrl Pts',(56.5615607032709,-3.46604029327769,331.507927587063));
#62654=CARTESIAN_POINT('Ctrl Pts',(56.553813624893,-3.56216353362662,331.606033977481));
#62655=CARTESIAN_POINT('Ctrl Pts',(56.5460665465152,-3.65401615175325,331.707987086109));
#62656=CARTESIAN_POINT('Ctrl Pts',(56.5383194032094,-3.74586953969322,331.809941049202));
#62657=CARTESIAN_POINT('Ctrl Pts',(56.5305722599036,-3.83345197239091,331.91574150441));
#62658=CARTESIAN_POINT('Ctrl Pts',(56.5228251165978,-3.91643789897057,332.024987857839));
#62659=CARTESIAN_POINT('Ctrl Pts',(56.5150762315697,-3.99944248254826,332.134258772167));
#62660=CARTESIAN_POINT('Ctrl Pts',(56.5073273465416,-4.07784826728229,332.24697681511));
#62661=CARTESIAN_POINT('Ctrl Pts',(56.4995784615135,-4.15137191752904,332.362710811297));
#62662=CARTESIAN_POINT('Ctrl Pts',(56.4918213517388,-4.22497360653796,332.478567648743));
#62663=CARTESIAN_POINT('Ctrl Pts',(56.484064241964,-4.29368259970469,332.59744650361));
#62664=CARTESIAN_POINT('Ctrl Pts',(56.4763071321892,-4.35726032634769,332.718889412822));
#62665=CARTESIAN_POINT('Ctrl Pts',(56.4685458772631,-4.42087202689499,332.840397217241));
#62666=CARTESIAN_POINT('Ctrl Pts',(56.4607846223369,-4.47934683071558,332.964471452755));
#62667=CARTESIAN_POINT('Ctrl Pts',(56.4530233674108,-4.53249400166833,333.090633302024));
#62668=CARTESIAN_POINT('Ctrl Pts',(56.4452496970061,-4.58572619077395,333.216996969135));
#62669=CARTESIAN_POINT('Ctrl Pts',(56.4374760266014,-4.63361357997391,333.34545455687));
#62670=CARTESIAN_POINT('Ctrl Pts',(56.4297023561968,-4.67601479227158,333.475510339505));
#62671=CARTESIAN_POINT('Ctrl Pts',(56.4222905520197,-4.71644221793553,333.599511994168));
#62672=CARTESIAN_POINT('Ctrl Pts',(56.4148787478426,-4.75188265712274,333.724966123298));
#62673=CARTESIAN_POINT('Ctrl Pts',(56.4074669436656,-4.78225706964697,333.851435512341));
#62674=CARTESIAN_POINT('Ctrl Pts',(56.3965253491456,-4.82709696256397,334.038134559028));
#62675=CARTESIAN_POINT('Ctrl Pts',(56.3855837546257,-4.8610201363199,334.227549293209));
#62676=CARTESIAN_POINT('Ctrl Pts',(56.3746421601057,-4.88376345013037,334.41858996769));
#62677=CARTESIAN_POINT('Ctrl Pts',(56.3644648444204,-4.90491812589157,334.596286303392));
#62678=CARTESIAN_POINT('Ctrl Pts',(56.354287528735,-4.91640065640646,334.775389583627));
#62679=CARTESIAN_POINT('Ctrl Pts',(56.3441102130496,-4.91804411929726,334.954998853952));
#62680=CARTESIAN_POINT('Ctrl Pts',(56.343345934215,-4.9181675372929,334.968486847059));
#62681=CARTESIAN_POINT('Ctrl Pts',(56.3425816553804,-4.91823548922244,334.981977680854));
#62682=CARTESIAN_POINT('Ctrl Pts',(56.3418173765457,-4.91824791469108,334.995470967337));
#62683=CARTESIAN_POINT('',(54.5918173764761,-4.91824995138137,335.000691546911));
#62684=CARTESIAN_POINT('Ctrl Pts',(56.3418173765086,-4.91824791469168,334.995470967994));
#62685=CARTESIAN_POINT('Ctrl Pts',(56.3341582515252,-4.91837243495727,335.130692254957));
#62686=CARTESIAN_POINT('Ctrl Pts',(56.3264991265419,-4.91291614338096,335.266068753081));
#62687=CARTESIAN_POINT('Ctrl Pts',(56.3188400015585,-4.90186747110353,335.401096445057));
#62688=CARTESIAN_POINT('Ctrl Pts',(56.3109395393849,-4.89047065781402,335.540378827203));
#62689=CARTESIAN_POINT('Ctrl Pts',(56.3030390772113,-4.87312317390013,335.679289627408));
#62690=CARTESIAN_POINT('Ctrl Pts',(56.2951386150377,-4.84987048605147,335.817275553915));
#62691=CARTESIAN_POINT('Ctrl Pts',(56.2874875112519,-4.82735171131172,335.950906298734));
#62692=CARTESIAN_POINT('Ctrl Pts',(56.2798364074662,-4.79929494347988,336.083669245075));
#62693=CARTESIAN_POINT('Ctrl Pts',(56.2721853036804,-4.76579405557933,336.215067933206));
#62694=CARTESIAN_POINT('Ctrl Pts',(56.2645351706831,-4.73229741834303,336.34644994919));
#62695=CARTESIAN_POINT('Ctrl Pts',(56.2568850376858,-4.69335813369513,336.476467662015));
#62696=CARTESIAN_POINT('Ctrl Pts',(56.2492349046884,-4.64912076540291,336.604636772357));
#62697=CARTESIAN_POINT('Ctrl Pts',(56.2415839872594,-4.60487886108559,336.732819024943));
#62698=CARTESIAN_POINT('Ctrl Pts',(56.2339330698303,-4.55533792414488,336.859151918501));
#62699=CARTESIAN_POINT('Ctrl Pts',(56.2262821524012,-4.50069158786027,336.983168750627));
#62700=CARTESIAN_POINT('Ctrl Pts',(56.21862869494,-4.44602710950884,337.107226755168));
#62701=CARTESIAN_POINT('Ctrl Pts',(56.2109752374786,-4.38625402331418,337.228966802032));
#62702=CARTESIAN_POINT('Ctrl Pts',(56.2033217800173,-4.32161281349888,337.34794500632));
#62703=CARTESIAN_POINT('Ctrl Pts',(56.1956599813704,-4.25690115391134,337.467052880015));
#62704=CARTESIAN_POINT('Ctrl Pts',(56.1879981827234,-4.1873109740053,337.583392551033));
#62705=CARTESIAN_POINT('Ctrl Pts',(56.1803363840764,-4.11312728368153,337.696547238736));
#62706=CARTESIAN_POINT('Ctrl Pts',(56.1726695744164,-4.03889507532004,337.809775932509));
#62707=CARTESIAN_POINT('Ctrl Pts',(56.1650027647564,-3.96006360955949,337.919815171335));
#62708=CARTESIAN_POINT('Ctrl Pts',(56.1573359550964,-3.87695858740802,338.026280749373));
#62709=CARTESIAN_POINT('Ctrl Pts',(56.1496584941899,-3.79373811018218,338.132894236537));
#62710=CARTESIAN_POINT('Ctrl Pts',(56.1419810332834,-3.7062324894227,338.235923852889));
#62711=CARTESIAN_POINT('Ctrl Pts',(56.1343035723768,-3.61480482110838,338.335021614292));
#62712=CARTESIAN_POINT('Ctrl Pts',(56.1326120180485,-3.59466080866041,338.356855557736));
#62713=CARTESIAN_POINT('Ctrl Pts',(56.1309204637201,-3.57432653234455,338.378498786957));
#62714=CARTESIAN_POINT('Ctrl Pts',(56.1292289093917,-3.55380608746057,338.399947845957));
#62715=CARTESIAN_POINT('Ctrl Pts',(56.1214538306133,-3.45948569061267,338.498536534865));
#62716=CARTESIAN_POINT('Ctrl Pts',(56.1136787518349,-3.36091061132691,338.593353124064));
#62717=CARTESIAN_POINT('Ctrl Pts',(56.1059036730564,-3.25841473465418,338.68400820839));
#62718=CARTESIAN_POINT('Ctrl Pts',(56.0981381620074,-3.1560449856829,338.774551735864));
#62719=CARTESIAN_POINT('Ctrl Pts',(56.0903726509584,-3.04976432925985,338.860943691297));
#62720=CARTESIAN_POINT('Ctrl Pts',(56.0826071399094,-2.9399450680366,338.942829702058));
#62721=CARTESIAN_POINT('Ctrl Pts',(56.0748493283872,-2.83023469293087,339.0246345226));
#62722=CARTESIAN_POINT('Ctrl Pts',(56.067091516865,-2.71699300654682,339.101942057215));
#62723=CARTESIAN_POINT('Ctrl Pts',(56.0593337053428,-2.60062685651415,339.174436850124));
#62724=CARTESIAN_POINT('Ctrl Pts',(56.0515817318198,-2.4843482756998,339.246877088403));
#62725=CARTESIAN_POINT('Ctrl Pts',(56.0438297582968,-2.36495024172537,339.314511588024));
#62726=CARTESIAN_POINT('Ctrl Pts',(56.0360777847739,-2.24286987932212,339.377067256386));
#62727=CARTESIAN_POINT('Ctrl Pts',(56.0283290942162,-2.12084121802434,339.439596432386));
#62728=CARTESIAN_POINT('Ctrl Pts',(56.0205804036586,-1.99613283479763,339.497050877214));
#62729=CARTESIAN_POINT('Ctrl Pts',(56.012831713101,-1.86920764438197,339.549202770232));
#62730=CARTESIAN_POINT('Ctrl Pts',(56.0050846347231,-1.74230886181227,339.601343812613));
#62731=CARTESIAN_POINT('Ctrl Pts',(55.9973375563453,-1.61319455078081,339.648184349146));
#62732=CARTESIAN_POINT('Ctrl Pts',(55.9895904779675,-1.48234848918881,339.68954432958));
#62733=CARTESIAN_POINT('Ctrl Pts',(55.9818433346616,-1.35150133098089,339.730904656651));
#62734=CARTESIAN_POINT('Ctrl Pts',(55.9740961913558,-1.21892276596177,339.766784218199));
#62735=CARTESIAN_POINT('Ctrl Pts',(55.96634904805,-1.0851122661618,339.797052681838));
#62736=CARTESIAN_POINT('Ctrl Pts',(55.9586001630219,-0.951271682920421,
339.82732795047));
#62737=CARTESIAN_POINT('Ctrl Pts',(55.9508512779938,-0.816198994936311,
339.85198952474));
#62738=CARTESIAN_POINT('Ctrl Pts',(55.9431023929657,-0.680404018054023,
339.870958163926));
#62739=CARTESIAN_POINT('Ctrl Pts',(55.935345283191,-0.544464906980432,339.889946936622));
#62740=CARTESIAN_POINT('Ctrl Pts',(55.9275881734162,-0.407802363290806,
339.903230649533));
#62741=CARTESIAN_POINT('Ctrl Pts',(55.9198310636415,-0.270932037427168,
339.910781902467));
#62742=CARTESIAN_POINT('Ctrl Pts',(55.9120698087153,-0.133988572437559,
339.918337190549));
#62743=CARTESIAN_POINT('Ctrl Pts',(55.9043085537891,0.00316250532587717,
339.920153909691));
#62744=CARTESIAN_POINT('Ctrl Pts',(55.896547298863,0.14000638281425,339.916256835772));
#62745=CARTESIAN_POINT('Ctrl Pts',(55.8887736284583,0.277069165909103,339.912353527804));
#62746=CARTESIAN_POINT('Ctrl Pts',(55.8809999580537,0.413823376612783,339.90271818942));
#62747=CARTESIAN_POINT('Ctrl Pts',(55.873226287649,0.549759262217033,339.887427525407));
#62748=CARTESIAN_POINT('Ctrl Pts',(55.8658144834719,0.679367299642118,339.872848645483));
#62749=CARTESIAN_POINT('Ctrl Pts',(55.8584026792948,0.808231199029922,339.853129145481));
#62750=CARTESIAN_POINT('Ctrl Pts',(55.8509908751177,0.935920287095614,339.828378224487));
#62751=CARTESIAN_POINT('Ctrl Pts',(55.8432157963393,1.06986779773376,339.802414187127));
#62752=CARTESIAN_POINT('Ctrl Pts',(55.8354407175609,1.20294572205231,339.770830996938));
#62753=CARTESIAN_POINT('Ctrl Pts',(55.8276656387824,1.3346459165838,339.733698695507));
#62754=CARTESIAN_POINT('Ctrl Pts',(55.8199001277334,1.46618404564138,339.696612087737));
#62755=CARTESIAN_POINT('Ctrl Pts',(55.8121346166844,1.59634744562955,339.653990060607));
#62756=CARTESIAN_POINT('Ctrl Pts',(55.8043691056354,1.72463664271504,339.605953919994));
#62757=CARTESIAN_POINT('Ctrl Pts',(55.7966112941132,1.85279864068811,339.557965407354));
#62758=CARTESIAN_POINT('Ctrl Pts',(55.788853482591,1.97908977013931,339.504573600254));
#62759=CARTESIAN_POINT('Ctrl Pts',(55.7810956710688,2.10302458897682,339.445949914322));
#62760=CARTESIAN_POINT('Ctrl Pts',(55.7733436975458,2.22686614293313,339.387370344573));
#62761=CARTESIAN_POINT('Ctrl Pts',(55.7655917240228,2.34835456382472,339.323566899169));
#62762=CARTESIAN_POINT('Ctrl Pts',(55.7578397504998,2.46702364898416,339.254759379548));
#62763=CARTESIAN_POINT('Ctrl Pts',(55.7500910599421,2.58564247771533,339.185980999953));
#62764=CARTESIAN_POINT('Ctrl Pts',(55.7423423693845,2.70144400803694,339.112202956792));
#62765=CARTESIAN_POINT('Ctrl Pts',(55.7345936788269,2.81398615098719,339.033691238128));
#62766=CARTESIAN_POINT('Ctrl Pts',(55.7268466004491,2.92650487860456,338.955195854483));
#62767=CARTESIAN_POINT('Ctrl Pts',(55.7190995220712,3.03576524735114,338.871968977832));
#62768=CARTESIAN_POINT('Ctrl Pts',(55.7113524436934,3.14135404914752,338.784319991809));
#62769=CARTESIAN_POINT('Ctrl Pts',(55.7036053003876,3.24694373588011,338.696670271203));
#62770=CARTESIAN_POINT('Ctrl Pts',(55.6958581570817,3.34886149353085,338.604598616961));
#62771=CARTESIAN_POINT('Ctrl Pts',(55.6881110137759,3.44672742984101,338.508454515436));
#62772=CARTESIAN_POINT('Ctrl Pts',(55.6803621287478,3.54461536849108,338.412288798676));
#62773=CARTESIAN_POINT('Ctrl Pts',(55.6726132437198,3.63844939436345,338.312049086619));
#62774=CARTESIAN_POINT('Ctrl Pts',(55.6648643586917,3.72788698163816,338.208121212584));
#62775=CARTESIAN_POINT('Ctrl Pts',(55.657107248917,3.81741949889219,338.10408302843));
#62776=CARTESIAN_POINT('Ctrl Pts',(55.6493501391422,3.90254600056036,337.996349159149));
#62777=CARTESIAN_POINT('Ctrl Pts',(55.6415930293675,3.982964397194,337.885338398383));
#62778=CARTESIAN_POINT('Ctrl Pts',(55.6338317744413,4.06342576684751,337.774268317016));
#62779=CARTESIAN_POINT('Ctrl Pts',(55.6260705195151,4.13917380263726,337.659918180706));
#62780=CARTESIAN_POINT('Ctrl Pts',(55.618309264589,4.20995074424667,337.542734314378));
#62781=CARTESIAN_POINT('Ctrl Pts',(55.6105355941843,4.28084090589646,337.425362992054));
#62782=CARTESIAN_POINT('Ctrl Pts',(55.6027619237796,4.3467438946554,337.305149224275));
#62783=CARTESIAN_POINT('Ctrl Pts',(55.594988253375,4.40744835677482,337.18256318233));
#62784=CARTESIAN_POINT('Ctrl Pts',(55.5875764491979,4.46532701157748,337.065683550131));
#62785=CARTESIAN_POINT('Ctrl Pts',(55.5801646450209,4.51848011349623,336.94664779499));
#62786=CARTESIAN_POINT('Ctrl Pts',(55.5727528408439,4.56676642834532,336.825877173152));
#62787=CARTESIAN_POINT('Ctrl Pts',(55.5649777620655,4.61741939932305,336.69918722338));
#62788=CARTESIAN_POINT('Ctrl Pts',(55.557202683287,4.66287652175415,336.570187681274));
#62789=CARTESIAN_POINT('Ctrl Pts',(55.5494276045086,4.70292170951451,336.439343759036));
#62790=CARTESIAN_POINT('Ctrl Pts',(55.5416620934596,4.74291761912187,336.308660848576));
#62791=CARTESIAN_POINT('Ctrl Pts',(55.5338965824106,4.77751473171469,336.17613844408));
#62792=CARTESIAN_POINT('Ctrl Pts',(55.5261310713616,4.80654476204257,336.042262209322));
#62793=CARTESIAN_POINT('Ctrl Pts',(55.5183732598395,4.83554600901076,335.908518713241));
#62794=CARTESIAN_POINT('Ctrl Pts',(55.5106154483173,4.85899107608548,335.77342443774));
#62795=CARTESIAN_POINT('Ctrl Pts',(55.5028576367951,4.87676140975535,335.637480364263));
#62796=CARTESIAN_POINT('Ctrl Pts',(55.4951056632721,4.89451837068569,335.501638593011));
#62797=CARTESIAN_POINT('Ctrl Pts',(55.4873536897491,4.90660904780779,335.364948682693));
#62798=CARTESIAN_POINT('Ctrl Pts',(55.4796017162261,4.91296598782485,335.227921620247));
#62799=CARTESIAN_POINT('Ctrl Pts',(55.4718530256685,4.91932023567402,335.090952588844));
#62800=CARTESIAN_POINT('Ctrl Pts',(55.4641043351109,4.91994555794236,334.953647078942));
#62801=CARTESIAN_POINT('Ctrl Pts',(55.4563556445532,4.91482638996126,334.816520793984));
#62802=CARTESIAN_POINT('Ctrl Pts',(55.4486085661754,4.90970828706581,334.679423039294));
#62803=CARTESIAN_POINT('Ctrl Pts',(55.4408614877976,4.89884808580942,334.542504825734));
#62804=CARTESIAN_POINT('Ctrl Pts',(55.4331144094198,4.88228234289008,334.40628105403));
#62805=CARTESIAN_POINT('Ctrl Pts',(55.425367266114,4.86571646113385,334.27005614064));
#62806=CARTESIAN_POINT('Ctrl Pts',(55.4176201228081,4.84344498952357,334.134526068731));
#62807=CARTESIAN_POINT('Ctrl Pts',(55.4098729795023,4.81555623709075,334.000199424927));
#62808=CARTESIAN_POINT('Ctrl Pts',(55.4021240944742,4.78766121467436,333.865842581642));
#62809=CARTESIAN_POINT('Ctrl Pts',(55.3943752094461,4.75414647788029,333.732690087478));
#62810=CARTESIAN_POINT('Ctrl Pts',(55.386626324418,4.71515112180248,333.601238776251));
#62811=CARTESIAN_POINT('Ctrl Pts',(55.3788692146433,4.67611437565081,333.469647941244));
#62812=CARTESIAN_POINT('Ctrl Pts',(55.3711121048686,4.63158550118186,333.339762271461));
#62813=CARTESIAN_POINT('Ctrl Pts',(55.3633549950939,4.58175319296852,333.212062433634));
#62814=CARTESIAN_POINT('Ctrl Pts',(55.3555937401677,4.53189425596296,333.084294357097));
#62815=CARTESIAN_POINT('Ctrl Pts',(55.3478324852415,4.47672639537413,332.958714797621));
#62816=CARTESIAN_POINT('Ctrl Pts',(55.3400712303154,4.41648544645576,332.835782043383));
#62817=CARTESIAN_POINT('Ctrl Pts',(55.3322975599107,4.35614813165165,332.712652636802));
#62818=CARTESIAN_POINT('Ctrl Pts',(55.3245238895061,4.29072169840841,332.592178839966));
#62819=CARTESIAN_POINT('Ctrl Pts',(55.3167502191014,4.22048714815252,332.474792821415));
#62820=CARTESIAN_POINT('Ctrl Pts',(55.3093384149243,4.15352203310783,332.362871150267));
#62821=CARTESIAN_POINT('Ctrl Pts',(55.3019266107471,4.08218652046496,332.253756495513));
#62822=CARTESIAN_POINT('Ctrl Pts',(55.29451480657,4.0067584236649,332.147795589918));
#62823=CARTESIAN_POINT('Ctrl Pts',(55.2867397277915,3.92763337115265,332.0366412247));
#62824=CARTESIAN_POINT('Ctrl Pts',(55.2789646490131,3.84375436138737,331.928606306436));
#62825=CARTESIAN_POINT('Ctrl Pts',(55.2711895702346,3.75539566463496,331.824124299576));
#62826=CARTESIAN_POINT('Ctrl Pts',(55.2634240591856,3.66714569888416,331.719770864478));
#62827=CARTESIAN_POINT('Ctrl Pts',(55.2556585481366,3.57442726450781,331.618961937195));
#62828=CARTESIAN_POINT('Ctrl Pts',(55.2478930370876,3.47755769772876,331.522101852919));
#62829=CARTESIAN_POINT('Ctrl Pts',(55.2401352255654,3.38078417740746,331.425337805699));
#62830=CARTESIAN_POINT('Ctrl Pts',(55.2323774140432,3.27986799010021,331.332515084436));
#62831=CARTESIAN_POINT('Ctrl Pts',(55.2246196025211,3.17516626568361,331.244004493112));
#62832=CARTESIAN_POINT('Ctrl Pts',(55.2168676289981,3.07054333263469,331.155560508814));
#62833=CARTESIAN_POINT('Ctrl Pts',(55.2091156554751,2.96214083005063,331.07142244674));
#62834=CARTESIAN_POINT('Ctrl Pts',(55.2013636819521,2.8503519549001,330.99192355416));
#62835=CARTESIAN_POINT('Ctrl Pts',(55.1936149913945,2.73861042240456,330.912458329408));
#62836=CARTESIAN_POINT('Ctrl Pts',(55.1858663008369,2.62348568760364,330.837628592575));
#62837=CARTESIAN_POINT('Ctrl Pts',(55.1781176102793,2.50540299358856,330.767726509048));
#62838=CARTESIAN_POINT('Ctrl Pts',(55.1703705319014,2.38734486766413,330.697838969232));
#62839=CARTESIAN_POINT('Ctrl Pts',(55.1626234535236,2.26633034280122,330.632877242438));
#62840=CARTESIAN_POINT('Ctrl Pts',(55.1548763751457,2.14281219293304,330.573089229687));
#62841=CARTESIAN_POINT('Ctrl Pts',(55.1471292318399,2.01929300786379,330.513300715854));
#62842=CARTESIAN_POINT('Ctrl Pts',(55.1393820885341,1.89327050776298,330.458686172848));
#62843=CARTESIAN_POINT('Ctrl Pts',(55.1316349452283,1.76522016305758,330.409446565126));
#62844=CARTESIAN_POINT('Ctrl Pts',(55.1238860602002,1.63714102991557,330.360195887294));
#62845=CARTESIAN_POINT('Ctrl Pts',(55.116137175172,1.50703350973344,330.316322689589));
#62846=CARTESIAN_POINT('Ctrl Pts',(55.1083882901439,1.37539067300435,330.277978869264));
#62847=CARTESIAN_POINT('Ctrl Pts',(55.1006311803692,1.24360810920885,330.239594350413));
#62848=CARTESIAN_POINT('Ctrl Pts',(55.0928740705945,1.11028734945773,330.206751042178));
#62849=CARTESIAN_POINT('Ctrl Pts',(55.0851169608197,0.975934710121021,330.179550383618));
#62850=CARTESIAN_POINT('Ctrl Pts',(55.0773557058936,0.841510277029617,330.152335189895));
#62851=CARTESIAN_POINT('Ctrl Pts',(55.0695944509674,0.706053251448218,330.130768715433));
#62852=CARTESIAN_POINT('Ctrl Pts',(55.0618331960412,0.570076641669434,330.114900647364));
#62853=CARTESIAN_POINT('Ctrl Pts',(55.0540595256366,0.433882513629586,330.099007195558));
#62854=CARTESIAN_POINT('Ctrl Pts',(55.0462858552319,0.297167530478643,330.088830394832));
#62855=CARTESIAN_POINT('Ctrl Pts',(55.0385121848272,0.160447177956737,330.084367816284));
#62856=CARTESIAN_POINT('Ctrl Pts',(55.0311003806502,0.0300911907387572,
330.080112971841));
#62857=CARTESIAN_POINT('Ctrl Pts',(55.0236885764732,-0.100269389422622,
330.081052325614));
#62858=CARTESIAN_POINT('Ctrl Pts',(55.0162767722961,-0.230192646753969,
330.087139895348));
#62859=CARTESIAN_POINT('Ctrl Pts',(55.0085016935177,-0.366483829949416,
330.093525835009));
#62860=CARTESIAN_POINT('Ctrl Pts',(55.0007266147393,-0.50272444270147,330.105597590486));
#62861=CARTESIAN_POINT('Ctrl Pts',(54.9929515359609,-0.63840155212901,330.123359094547));
#62862=CARTESIAN_POINT('Ctrl Pts',(54.9851860249118,-0.773911702235956,
330.141098741946));
#62863=CARTESIAN_POINT('Ctrl Pts',(54.9774205138628,-0.908859344876275,
330.164514156507));
#62864=CARTESIAN_POINT('Ctrl Pts',(54.9696550028138,-1.04273273712167,330.193557292401));
#62865=CARTESIAN_POINT('Ctrl Pts',(54.9618971912916,-1.17647339350881,330.222571631941));
#62866=CARTESIAN_POINT('Ctrl Pts',(54.9541393797694,-1.309141539627,330.257202506158));
#62867=CARTESIAN_POINT('Ctrl Pts',(54.9463815682472,-1.4402320950282,330.297350260231));
#62868=CARTESIAN_POINT('Ctrl Pts',(54.9386295947241,-1.57122400062969,330.337467801846));
#62869=CARTESIAN_POINT('Ctrl Pts',(54.9308776212012,-1.70064030631718,330.383093845706));
#62870=CARTESIAN_POINT('Ctrl Pts',(54.9231256476781,-1.8279879959111,330.434078083311));
#62871=CARTESIAN_POINT('Ctrl Pts',(54.9153769571205,-1.95528175368235,330.48504072906));
#62872=CARTESIAN_POINT('Ctrl Pts',(54.9076282665629,-2.08050827566386,330.541356910303));
#62873=CARTESIAN_POINT('Ctrl Pts',(54.8998795760052,-2.20319175031282,330.602827138507));
#62874=CARTESIAN_POINT('Ctrl Pts',(54.8921324976274,-2.32584969964054,330.664284577316));
#62875=CARTESIAN_POINT('Ctrl Pts',(54.8843854192495,-2.44596530481481,330.730893755133));
#62876=CARTESIAN_POINT('Ctrl Pts',(54.8766383408717,-2.56308507862277,330.802408078167));
#62877=CARTESIAN_POINT('Ctrl Pts',(54.8688911975659,-2.68020583400715,330.873923000558));
#62878=CARTESIAN_POINT('Ctrl Pts',(54.8611440542601,-2.79433037434501,330.950342946463));
#62879=CARTESIAN_POINT('Ctrl Pts',(54.8533969109542,-2.90503240000683,331.031376836054));
#62880=CARTESIAN_POINT('Ctrl Pts',(54.8456480259262,-3.01575931383354,331.112428943783));
#62881=CARTESIAN_POINT('Ctrl Pts',(54.8378991408981,-3.12306186651507,331.198096828503));
#62882=CARTESIAN_POINT('Ctrl Pts',(54.8301502558701,-3.22654549567289,331.288048057039));
#62883=CARTESIAN_POINT('Ctrl Pts',(54.8223931460953,-3.33013896342452,331.378094760739));
#62884=CARTESIAN_POINT('Ctrl Pts',(54.8146360363206,-3.42990511504537,331.472433633252));
#62885=CARTESIAN_POINT('Ctrl Pts',(54.8068789265458,-3.52548465142783,331.570693796838));
#62886=CARTESIAN_POINT('Ctrl Pts',(54.7991176716197,-3.62111526245843,331.669006467513));
#62887=CARTESIAN_POINT('Ctrl Pts',(54.7913564166935,-3.71255453999873,331.771244313358));
#62888=CARTESIAN_POINT('Ctrl Pts',(54.7835951617674,-3.79948308285538,331.877002823313));
#62889=CARTESIAN_POINT('Ctrl Pts',(54.7758214913627,-3.88655068305071,331.982930512418));
#62890=CARTESIAN_POINT('Ctrl Pts',(54.7680478209581,-3.96909289398145,332.092389807617));
#62891=CARTESIAN_POINT('Ctrl Pts',(54.7602741505534,-4.04683279924899,332.204945911539));
#62892=CARTESIAN_POINT('Ctrl Pts',(54.7528623463762,-4.12095389322377,332.312262501744));
#62893=CARTESIAN_POINT('Ctrl Pts',(54.7454505421991,-4.19070956061081,332.422393832951));
#62894=CARTESIAN_POINT('Ctrl Pts',(54.7380387380219,-4.25589932288684,332.534943405122));
#62895=CARTESIAN_POINT('Ctrl Pts',(54.7299509628006,-4.32703451904377,332.657757718508));
#62896=CARTESIAN_POINT('Ctrl Pts',(54.7218631875793,-4.39294259267623,332.783813504407));
#62897=CARTESIAN_POINT('Ctrl Pts',(54.713775412358,-4.4533284598564,332.912645528155));
#62898=CARTESIAN_POINT('Ctrl Pts',(54.7057004306988,-4.51361880628807,333.041273760321));
#62899=CARTESIAN_POINT('Ctrl Pts',(54.6976254490397,-4.56840420158663,333.172669170312));
#62900=CARTESIAN_POINT('Ctrl Pts',(54.6895504673805,-4.61743424595299,333.306340043928));
#62901=CARTESIAN_POINT('Ctrl Pts',(54.6814060431412,-4.66688593496565,333.441160449612));
#62902=CARTESIAN_POINT('Ctrl Pts',(54.6732616189019,-4.71048260241859,333.578295351565));
#62903=CARTESIAN_POINT('Ctrl Pts',(54.6651171946625,-4.74801496691996,333.717215163637));
#62904=CARTESIAN_POINT('Ctrl Pts',(54.6570678915408,-4.78510897993681,333.85451249051));
#62905=CARTESIAN_POINT('Ctrl Pts',(54.649018588419,-4.81627946047852,333.993552920156));
#62906=CARTESIAN_POINT('Ctrl Pts',(54.6409692852972,-4.84137278189544,334.133805651587));
#62907=CARTESIAN_POINT('Ctrl Pts',(54.6327773004991,-4.86691090668357,334.276544498217));
#62908=CARTESIAN_POINT('Ctrl Pts',(54.624585315701,-4.88615423912597,334.420538700199));
#62909=CARTESIAN_POINT('Ctrl Pts',(54.6163933309029,-4.8989941346828,334.565213235202));
#62910=CARTESIAN_POINT('Ctrl Pts',(54.6082013461048,-4.91183403023962,334.709887770205));
#62911=CARTESIAN_POINT('Ctrl Pts',(54.6000093613067,-4.91827040274491,334.855242264824));
#62912=CARTESIAN_POINT('Ctrl Pts',(54.5918173765086,-4.91824995138145,335.000691546333));
#62913=CARTESIAN_POINT('',(52.8418173765483,-4.9182481654623,335.0042479909));
#62914=CARTESIAN_POINT('Ctrl Pts',(54.5918173764761,-4.91824995138137,335.000691546911));
#62915=CARTESIAN_POINT('Ctrl Pts',(54.5836110677012,-4.91822946424087,335.146395151661));
#62916=CARTESIAN_POINT('Ctrl Pts',(54.5754047589264,-4.91172998599915,335.291945594707));
#62917=CARTESIAN_POINT('Ctrl Pts',(54.5671984501516,-4.89881778224724,335.436769274146));
#62918=CARTESIAN_POINT('Ctrl Pts',(54.5589779382225,-4.88588323056439,335.581843608675));
#62919=CARTESIAN_POINT('Ctrl Pts',(54.5507574262934,-4.86651382143102,335.726188354007));
#62920=CARTESIAN_POINT('Ctrl Pts',(54.5425369143643,-4.84082709624967,335.86923879729));
#62921=CARTESIAN_POINT('Ctrl Pts',(54.5342938029828,-4.81506975430787,336.012682508257));
#62922=CARTESIAN_POINT('Ctrl Pts',(54.5260506916014,-4.782960419235,336.154824488968));
#62923=CARTESIAN_POINT('Ctrl Pts',(54.5178075802199,-4.74466735313486,336.295111875707));
#62924=CARTESIAN_POINT('Ctrl Pts',(54.5095521161366,-4.70631690301917,336.435609489894));
#62925=CARTESIAN_POINT('Ctrl Pts',(54.5012966520531,-4.66176431752209,336.574246661269));
#62926=CARTESIAN_POINT('Ctrl Pts',(54.4930411879697,-4.61122656490549,336.710489003066));
#62927=CARTESIAN_POINT('Ctrl Pts',(54.4847663984023,-4.56057050682228,336.847050278987));
#62928=CARTESIAN_POINT('Ctrl Pts',(54.4764916088349,-4.50390138954868,336.981205224612));
#62929=CARTESIAN_POINT('Ctrl Pts',(54.4682168192675,-4.44148355973158,337.112440969858));
#62930=CARTESIAN_POINT('Ctrl Pts',(54.4654114474277,-4.42032226968963,337.156933347711));
#62931=CARTESIAN_POINT('Ctrl Pts',(54.4626060755879,-4.3985006058219,337.201090428254));
#62932=CARTESIAN_POINT('Ctrl Pts',(54.4598007037481,-4.37603000737524,337.244892967839));
#62933=CARTESIAN_POINT('Ctrl Pts',(54.4520256249696,-4.31375281807674,337.366291561469));
#62934=CARTESIAN_POINT('Ctrl Pts',(54.4442505461912,-4.24632168263603,337.485288510239));
#62935=CARTESIAN_POINT('Ctrl Pts',(54.4364754674127,-4.17394552842669,337.601415343275));
#62936=CARTESIAN_POINT('Ctrl Pts',(54.4287099563637,-4.10165843768284,337.71739927485));
#62937=CARTESIAN_POINT('Ctrl Pts',(54.4209444453147,-4.02443864066394,337.830519789531));
#62938=CARTESIAN_POINT('Ctrl Pts',(54.4131789342657,-3.94254187962858,337.940331034063));
#62939=CARTESIAN_POINT('Ctrl Pts',(54.4054211227435,-3.86072631947018,338.050033400427));
#62940=CARTESIAN_POINT('Ctrl Pts',(54.3976633112213,-3.77424325580748,338.156432715007));
#62941=CARTESIAN_POINT('Ctrl Pts',(54.3899054996991,-3.68339264214193,338.25911056982));
#62942=CARTESIAN_POINT('Ctrl Pts',(54.3821535261761,-3.59261039644439,338.361711156292));
#62943=CARTESIAN_POINT('Ctrl Pts',(54.3744015526532,-3.49746740077174,338.460595565733));
#62944=CARTESIAN_POINT('Ctrl Pts',(54.3666495791302,-3.39830471245034,338.555377356039));
#62945=CARTESIAN_POINT('Ctrl Pts',(54.3589008885725,-3.29918401958624,338.650119006202));
#62946=CARTESIAN_POINT('Ctrl Pts',(54.3511521980149,-3.19604730188507,338.740761223404));
#62947=CARTESIAN_POINT('Ctrl Pts',(54.3434035074573,-3.0892732496295,338.826953599356));
#62948=CARTESIAN_POINT('Ctrl Pts',(54.3356564290795,-2.98252141260715,338.913128042265));
#62949=CARTESIAN_POINT('Ctrl Pts',(54.3279093507016,-2.87213405026839,338.994854240095));
#62950=CARTESIAN_POINT('Ctrl Pts',(54.3201622723237,-2.75852347643963,339.071821618444));
#62951=CARTESIAN_POINT('Ctrl Pts',(54.3124151290179,-2.64491195044507,339.148789641855));
#62952=CARTESIAN_POINT('Ctrl Pts',(54.3046679857122,-2.52807748268486,339.220998547002));
#62953=CARTESIAN_POINT('Ctrl Pts',(54.2969208424064,-2.40846161182988,339.28818093448));
#62954=CARTESIAN_POINT('Ctrl Pts',(54.2891719573783,-2.28881884878754,339.355378425986));
#62955=CARTESIAN_POINT('Ctrl Pts',(54.2814230723502,-2.16639377906995,339.417546959742));
#62956=CARTESIAN_POINT('Ctrl Pts',(54.2736741873221,-2.04165243009053,339.474465154318));
#62957=CARTESIAN_POINT('Ctrl Pts',(54.2659170775474,-1.91677867935449,339.531443762454));
#62958=CARTESIAN_POINT('Ctrl Pts',(54.2581599677726,-1.78958409439328,339.583160736775));
#62959=CARTESIAN_POINT('Ctrl Pts',(54.2504028579979,-1.66055508313776,339.629442717905));
#62960=CARTESIAN_POINT('Ctrl Pts',(54.2426416030717,-1.53145712290427,339.675749430646));
#62961=CARTESIAN_POINT('Ctrl Pts',(54.2348803481456,-1.4005231560564,339.716615246746));
#62962=CARTESIAN_POINT('Ctrl Pts',(54.2271190932194,-1.26825367200316,339.751917053774));
#62963=CARTESIAN_POINT('Ctrl Pts',(54.2193454228147,-1.13577259988187,339.787275332189));
#62964=CARTESIAN_POINT('Ctrl Pts',(54.2115717524101,-1.00195212315458,339.817051730551));
#62965=CARTESIAN_POINT('Ctrl Pts',(54.2037980820054,-0.867302694724706,
339.841174351149));
#62966=CARTESIAN_POINT('Ctrl Pts',(54.1963862778283,-0.738921229583391,
339.864174057954));
#62967=CARTESIAN_POINT('Ctrl Pts',(54.1889744736512,-0.60978653644116,339.882034468721));
#62968=CARTESIAN_POINT('Ctrl Pts',(54.1815626694742,-0.480342544192952,
339.894737388537));
#62969=CARTESIAN_POINT('Ctrl Pts',(54.1737875906957,-0.344554116290516,
339.908062916293));
#62970=CARTESIAN_POINT('Ctrl Pts',(54.1660125119173,-0.207996186796566,
339.915754712944));
#62971=CARTESIAN_POINT('Ctrl Pts',(54.1582374331389,-0.071175765453526,
339.917734953504));
#62972=CARTESIAN_POINT('Ctrl Pts',(54.1504719220899,0.0654762896507296,
339.919712757252));
#62973=CARTESIAN_POINT('Ctrl Pts',(54.1427064110408,0.202389806803813,339.915992983874));
#62974=CARTESIAN_POINT('Ctrl Pts',(54.1349408999918,0.339051461682754,339.906549415713));
#62975=CARTESIAN_POINT('Ctrl Pts',(54.1271830884696,0.475577616133003,339.897115210877));
#62976=CARTESIAN_POINT('Ctrl Pts',(54.1194252769474,0.611852017837889,339.881968531918));
#62977=CARTESIAN_POINT('Ctrl Pts',(54.1116674654252,0.747360496548205,339.861135191568));
#62978=CARTESIAN_POINT('Ctrl Pts',(54.1039154919022,0.882767000831071,339.840317528967));
#62979=CARTESIAN_POINT('Ctrl Pts',(54.0961635183792,1.0174083445987,339.813821782053));
#62980=CARTESIAN_POINT('Ctrl Pts',(54.0884115448561,1.15077499475336,339.781725627214));
#62981=CARTESIAN_POINT('Ctrl Pts',(54.0806628542985,1.28408516405241,339.749643065114));
#62982=CARTESIAN_POINT('Ctrl Pts',(54.0729141637409,1.41612133419609,339.711964903651));
#62983=CARTESIAN_POINT('Ctrl Pts',(54.0651654731833,1.54638390833746,339.66881996553));
#62984=CARTESIAN_POINT('Ctrl Pts',(54.0574183948055,1.67661938026239,339.625684004074));
#62985=CARTESIAN_POINT('Ctrl Pts',(54.0496713164276,1.80508161935684,339.577083651167));
#62986=CARTESIAN_POINT('Ctrl Pts',(54.0419242380497,1.93128633031,339.523197560671));
#62987=CARTESIAN_POINT('Ctrl Pts',(54.0341770947439,2.05749209897993,339.469311018558));
#62988=CARTESIAN_POINT('Ctrl Pts',(54.0264299514382,2.18143994229291,339.410138803985));
#62989=CARTESIAN_POINT('Ctrl Pts',(54.0186828081324,2.30266605647411,339.34590751108));
#62990=CARTESIAN_POINT('Ctrl Pts',(54.0109339231043,2.42391942485956,339.281661777616));
#62991=CARTESIAN_POINT('Ctrl Pts',(54.0031850380761,2.54244950117534,339.212354885512));
#62992=CARTESIAN_POINT('Ctrl Pts',(53.995436153048,2.65781792688049,339.138258924965));
#62993=CARTESIAN_POINT('Ctrl Pts',(53.9876790432733,2.77330880582467,339.064084318201));
#62994=CARTESIAN_POINT('Ctrl Pts',(53.9799219334986,2.88563100121114,338.985110700454));
#62995=CARTESIAN_POINT('Ctrl Pts',(53.9721648237238,2.99437550819959,338.901653287825));
#62996=CARTESIAN_POINT('Ctrl Pts',(53.9644035687977,3.1031781247756,338.818151278223));
#62997=CARTESIAN_POINT('Ctrl Pts',(53.9566423138715,3.20839894381921,338.730160950119));
#62998=CARTESIAN_POINT('Ctrl Pts',(53.9488810589453,3.30966359392258,338.638036552533));
#62999=CARTESIAN_POINT('Ctrl Pts',(53.9411073885407,3.41109023446403,338.545764785934));
#63000=CARTESIAN_POINT('Ctrl Pts',(53.933333718136,3.50854778167336,338.449346009842));
#63001=CARTESIAN_POINT('Ctrl Pts',(53.9255600477314,3.60169953987352,338.349170567017));
#63002=CARTESIAN_POINT('Ctrl Pts',(53.9181482435543,3.69051506131787,338.253658315157));
#63003=CARTESIAN_POINT('Ctrl Pts',(53.9107364393772,3.77541645397247,338.154731489822));
#63004=CARTESIAN_POINT('Ctrl Pts',(53.9033246352002,3.8561481819506,338.05275355398));
#63005=CARTESIAN_POINT('Ctrl Pts',(53.8955495564218,3.94083681240484,337.945777375726));
#63006=CARTESIAN_POINT('Ctrl Pts',(53.8877744776433,4.02120433964719,337.835105372002));
#63007=CARTESIAN_POINT('Ctrl Pts',(53.8799993988649,4.09691094692358,337.721121782552));
#63008=CARTESIAN_POINT('Ctrl Pts',(53.8722338878159,4.17252439239999,337.607278457165));
#63009=CARTESIAN_POINT('Ctrl Pts',(53.8644683767669,4.24348811583597,337.490131976854));
#63010=CARTESIAN_POINT('Ctrl Pts',(53.8567028657179,4.30950228099872,337.370099819115));
#63011=CARTESIAN_POINT('Ctrl Pts',(53.8489450541957,4.37545099292452,337.250186673609));
#63012=CARTESIAN_POINT('Ctrl Pts',(53.8411872426735,4.43645972563388,337.127393884827));
#63013=CARTESIAN_POINT('Ctrl Pts',(53.8334294311513,4.49227193857836,337.002167798253));
#63014=CARTESIAN_POINT('Ctrl Pts',(53.8256774576283,4.54804215106267,336.87703594828));
#63015=CARTESIAN_POINT('Ctrl Pts',(53.8179254841053,4.59862346905246,336.749474800878));
#63016=CARTESIAN_POINT('Ctrl Pts',(53.8101735105823,4.64380547468176,336.61995486845));
#63017=CARTESIAN_POINT('Ctrl Pts',(53.8024248200247,4.68896834570485,336.49048978779));
#63018=CARTESIAN_POINT('Ctrl Pts',(53.7946761294671,4.72873632380081,336.359067940308));
#63019=CARTESIAN_POINT('Ctrl Pts',(53.7869274389095,4.76294737821085,336.22617916101));
#63020=CARTESIAN_POINT('Ctrl Pts',(53.7791803605316,4.79715131472528,336.093318030331));
#63021=CARTESIAN_POINT('Ctrl Pts',(53.7714332821538,4.82580052985802,335.958990953209));
#63022=CARTESIAN_POINT('Ctrl Pts',(53.763686203776,4.8487831774724,335.823701863759));
#63023=CARTESIAN_POINT('Ctrl Pts',(53.7559390604702,4.8717660177035,335.688411640456));
#63024=CARTESIAN_POINT('Ctrl Pts',(53.7481919171644,4.88908213022821,335.552159774097));
#63025=CARTESIAN_POINT('Ctrl Pts',(53.7404447738586,4.90067107204616,335.415458910255));
#63026=CARTESIAN_POINT('Ctrl Pts',(53.7326958888305,4.91226261930427,335.278727313156));
#63027=CARTESIAN_POINT('Ctrl Pts',(53.7249470038024,4.91812440068441,335.141546907107));
#63028=CARTESIAN_POINT('Ctrl Pts',(53.7171981187743,4.91824800168097,335.004433560777));
#63029=CARTESIAN_POINT('Ctrl Pts',(53.7094410089996,4.9183717338689,334.867174680925));
#63030=CARTESIAN_POINT('Ctrl Pts',(53.7016838992249,4.91274511884748,334.729983394468));
#63031=CARTESIAN_POINT('Ctrl Pts',(53.6939267894502,4.90141189257198,334.59337422382));
#63032=CARTESIAN_POINT('Ctrl Pts',(53.686165534524,4.89007261018273,334.4566920536));
#63033=CARTESIAN_POINT('Ctrl Pts',(53.6784042795978,4.87302068884256,334.320593006657));
#63034=CARTESIAN_POINT('Ctrl Pts',(53.6706430246717,4.85035143026003,334.185583604368));
#63035=CARTESIAN_POINT('Ctrl Pts',(53.662869354267,4.82764590825166,334.050358231035));
#63036=CARTESIAN_POINT('Ctrl Pts',(53.6550956838624,4.7993051733402,333.91622636817));
#63037=CARTESIAN_POINT('Ctrl Pts',(53.6473220134577,4.76547526772822,333.783682387215));
#63038=CARTESIAN_POINT('Ctrl Pts',(53.6399102092806,4.73322015236124,333.657308360461));
#63039=CARTESIAN_POINT('Ctrl Pts',(53.6324984051034,4.69597548963163,333.532377986476));
#63040=CARTESIAN_POINT('Ctrl Pts',(53.6250866009263,4.65390863817244,333.409302841505));
#63041=CARTESIAN_POINT('Ctrl Pts',(53.6173115221479,4.60977996501279,333.280195417058));
#63042=CARTESIAN_POINT('Ctrl Pts',(53.6095364433694,4.56020499647602,333.15272167726));
#63043=CARTESIAN_POINT('Ctrl Pts',(53.601761364591,4.50532295361591,333.027375315444));
#63044=CARTESIAN_POINT('Ctrl Pts',(53.593995853542,4.45050844660351,332.902183200305));
#63045=CARTESIAN_POINT('Ctrl Pts',(53.586230342493,4.39040001474811,332.779113608963));
#63046=CARTESIAN_POINT('Ctrl Pts',(53.5784648314439,4.32518646519238,332.65864460113));
#63047=CARTESIAN_POINT('Ctrl Pts',(53.5707070199217,4.26003757506089,332.53829503867));
#63048=CARTESIAN_POINT('Ctrl Pts',(53.5629492083995,4.18979382525483,332.420541269912));
#63049=CARTESIAN_POINT('Ctrl Pts',(53.5551913968773,4.11469172840129,332.305840568428));
#63050=CARTESIAN_POINT('Ctrl Pts',(53.5474394233543,4.03964614825732,332.191226182861));
#63051=CARTESIAN_POINT('Ctrl Pts',(53.5396874498313,3.95974971152921,332.079660617142));
#63052=CARTESIAN_POINT('Ctrl Pts',(53.5319354763083,3.87528421295256,331.971575437403));
#63053=CARTESIAN_POINT('Ctrl Pts',(53.5241867857507,3.7908544855647,331.863536031802));
#63054=CARTESIAN_POINT('Ctrl Pts',(53.5164380951931,3.70185978508869,331.758974387952));
#63055=CARTESIAN_POINT('Ctrl Pts',(53.5086894046355,3.60862434008963,331.658291838803));
#63056=CARTESIAN_POINT('Ctrl Pts',(53.5009423262576,3.51540829350356,331.557630237499));
#63057=CARTESIAN_POINT('Ctrl Pts',(53.4931952478798,3.41795352280899,331.460846412172));
#63058=CARTESIAN_POINT('Ctrl Pts',(53.4854481695019,3.31662327059217,331.368307124292));
#63059=CARTESIAN_POINT('Ctrl Pts',(53.4777010261961,3.21529216913031,331.275767060844));
#63060=CARTESIAN_POINT('Ctrl Pts',(53.4699538828903,3.110085809988,331.187471869381));
#63061=CARTESIAN_POINT('Ctrl Pts',(53.4622067395845,3.00140257858864,331.103749799648));
#63062=CARTESIAN_POINT('Ctrl Pts',(53.4544578545564,2.89269491289152,331.020008907416));
#63063=CARTESIAN_POINT('Ctrl Pts',(53.4467089695283,2.78050912908314,330.940843421275));
#63064=CARTESIAN_POINT('Ctrl Pts',(53.4389600845002,2.6652744785608,330.866539583299));
#63065=CARTESIAN_POINT('Ctrl Pts',(53.4312029747255,2.54991751678973,330.792156878462));
#63066=CARTESIAN_POINT('Ctrl Pts',(53.4234458649507,2.43150555291668,330.722646341935));
#63067=CARTESIAN_POINT('Ctrl Pts',(53.415688755176,2.31049492785192,330.658249632824));
#63068=CARTESIAN_POINT('Ctrl Pts',(53.4079275002498,2.18941963857838,330.593818512171));
#63069=CARTESIAN_POINT('Ctrl Pts',(53.4001662453236,2.06574327338222,330.53450683295));
#63070=CARTESIAN_POINT('Ctrl Pts',(53.3924049903975,1.93994335011714,330.480508561703));
#63071=CARTESIAN_POINT('Ctrl Pts',(53.3846313199928,1.81394218797293,330.42642391082));
#63072=CARTESIAN_POINT('Ctrl Pts',(53.3768576495881,1.68581104506024,330.37766979195));
#63073=CARTESIAN_POINT('Ctrl Pts',(53.3690839791834,1.55604468068748,330.334390927842));
#63074=CARTESIAN_POINT('Ctrl Pts',(53.3616721750064,1.43231897179732,330.293126705271));
#63075=CARTESIAN_POINT('Ctrl Pts',(53.3542603708294,1.30710713094088,330.256839542874));
#63076=CARTESIAN_POINT('Ctrl Pts',(53.3468485666524,1.18084582872362,330.225611432729));
#63077=CARTESIAN_POINT('Ctrl Pts',(53.339073487874,1.04839608397063,330.192852739882));
#63078=CARTESIAN_POINT('Ctrl Pts',(53.3312984090956,0.914372836555685,330.165558033514));
#63079=CARTESIAN_POINT('Ctrl Pts',(53.3235233303171,0.779266584234283,330.143877405461));
#63080=CARTESIAN_POINT('Ctrl Pts',(53.3157578192681,0.644326588757556,330.1222234568));
#63081=CARTESIAN_POINT('Ctrl Pts',(53.3079923082191,0.508306622325505,330.106169901897));
#63082=CARTESIAN_POINT('Ctrl Pts',(53.3002267971701,0.371710869928192,330.09581667434));
#63083=CARTESIAN_POINT('Ctrl Pts',(53.2924689856479,0.235250552617069,330.085473712039));
#63084=CARTESIAN_POINT('Ctrl Pts',(53.2847111741257,0.0982159726965942,
330.08081985885));
#63085=CARTESIAN_POINT('Ctrl Pts',(53.2769533626035,-0.0388803481775629,
330.08190368323));
#63086=CARTESIAN_POINT('Ctrl Pts',(53.2692013890805,-0.175873499722502,
330.082986691998));
#63087=CARTESIAN_POINT('Ctrl Pts',(53.2614494155575,-0.312927910452457,
330.089798780917));
#63088=CARTESIAN_POINT('Ctrl Pts',(53.2536974420345,-0.44952817189983,330.102336527979));
#63089=CARTESIAN_POINT('Ctrl Pts',(53.2459487514769,-0.586070583055472,
330.114868965298));
#63090=CARTESIAN_POINT('Ctrl Pts',(53.2382000609192,-0.722158839036186,
330.133122202314));
#63091=CARTESIAN_POINT('Ctrl Pts',(53.2304513703616,-0.85727999172154,330.157040772596));
#63092=CARTESIAN_POINT('Ctrl Pts',(53.2227042919838,-0.992373031322524,
330.18095436642));
#63093=CARTESIAN_POINT('Ctrl Pts',(53.214957213606,-1.1264989832079,330.210530880865));
#63094=CARTESIAN_POINT('Ctrl Pts',(53.2072101352282,-1.25915285842844,330.245663333165));
#63095=CARTESIAN_POINT('Ctrl Pts',(53.1994629919224,-1.39180784541614,330.280796079909));
#63096=CARTESIAN_POINT('Ctrl Pts',(53.1917158486166,-1.5229903532837,330.321484757313));
#63097=CARTESIAN_POINT('Ctrl Pts',(53.1839687053107,-1.65220876060685,330.367571989348));
#63098=CARTESIAN_POINT('Ctrl Pts',(53.1762198202827,-1.78145621897136,330.413669582771));
#63099=CARTESIAN_POINT('Ctrl Pts',(53.1684709352546,-1.90873833002666,330.465168014688));
#63100=CARTESIAN_POINT('Ctrl Pts',(53.1607220502265,-2.03358209414407,330.521861220454));
#63101=CARTESIAN_POINT('Ctrl Pts',(53.1529649404518,-2.15855836872268,330.578614600973));
#63102=CARTESIAN_POINT('Ctrl Pts',(53.145207830677,-2.28109076995865,330.640573607775));
#63103=CARTESIAN_POINT('Ctrl Pts',(53.1374507209023,-2.40072912930451,330.707485269657));
#63104=CARTESIAN_POINT('Ctrl Pts',(53.1296894659761,-2.52043141956423,330.774432686993));
#63105=CARTESIAN_POINT('Ctrl Pts',(53.12192821105,-2.63723625373589,330.846337828076));
#63106=CARTESIAN_POINT('Ctrl Pts',(53.1141669561238,-2.75072210890685,330.922904104381));
#63107=CARTESIAN_POINT('Ctrl Pts',(53.1063932857192,-2.86438950446113,330.999592861776));
#63108=CARTESIAN_POINT('Ctrl Pts',(53.0986196153145,-2.97472699673653,331.080957422177));
#63109=CARTESIAN_POINT('Ctrl Pts',(53.0908459449099,-3.08134514263344,331.166660049713));
#63110=CARTESIAN_POINT('Ctrl Pts',(53.0834341407327,-3.1830001881896,331.248373199319));
#63111=CARTESIAN_POINT('Ctrl Pts',(53.0760223365555,-3.2812741489455,331.334029441844));
#63112=CARTESIAN_POINT('Ctrl Pts',(53.0686105323783,-3.37586176849261,331.42330594228));
#63113=CARTESIAN_POINT('Ctrl Pts',(53.0609503198048,-3.47361951481569,331.515574566059));
#63114=CARTESIAN_POINT('Ctrl Pts',(53.0532901072313,-3.56776814878884,331.61202089573));
#63115=CARTESIAN_POINT('Ctrl Pts',(53.0456298946578,-3.65792139769576,331.712326945881));
#63116=CARTESIAN_POINT('Ctrl Pts',(53.0379792275201,-3.74796230611111,331.812508004076));
#63117=CARTESIAN_POINT('Ctrl Pts',(53.0303285603824,-3.83401746346419,331.916538921007));
#63118=CARTESIAN_POINT('Ctrl Pts',(53.0226778932446,-3.91573487042647,332.024062586843));
#63119=CARTESIAN_POINT('Ctrl Pts',(53.0150358707388,-3.99735994336243,332.131464759679));
#63120=CARTESIAN_POINT('Ctrl Pts',(53.0073938482329,-4.07465677894538,332.242351507227));
#63121=CARTESIAN_POINT('Ctrl Pts',(52.9997518257271,-4.14731185508742,332.356330686498));
#63122=CARTESIAN_POINT('Ctrl Pts',(52.9921146466571,-4.21992088318378,332.470237626928));
#63123=CARTESIAN_POINT('Ctrl Pts',(52.9844774675871,-4.28789378438795,332.587232763907));
#63124=CARTESIAN_POINT('Ctrl Pts',(52.9768402885171,-4.35095889711398,332.70689299462));
#63125=CARTESIAN_POINT('Ctrl Pts',(52.9692061827568,-4.41399863153953,332.82650507235));
#63126=CARTESIAN_POINT('Ctrl Pts',(52.9615720769966,-4.47213431715448,332.94877975483));
#63127=CARTESIAN_POINT('Ctrl Pts',(52.9539379712363,-4.52513931028059,333.073267718376));
#63128=CARTESIAN_POINT('Ctrl Pts',(52.9463051715254,-4.57813523526711,333.197734384413));
#63129=CARTESIAN_POINT('Ctrl Pts',(52.9386723718145,-4.62600205673172,333.324413206935));
#63130=CARTESIAN_POINT('Ctrl Pts',(52.9310395721036,-4.66856075493242,333.452833706415));
#63131=CARTESIAN_POINT('Ctrl Pts',(52.9234031308337,-4.71113975761084,333.581315474479));
#63132=CARTESIAN_POINT('Ctrl Pts',(52.9157666895637,-4.74840544637987,333.71154019753));
#63133=CARTESIAN_POINT('Ctrl Pts',(52.9081302482938,-4.78022829497211,333.843020955052));
#63134=CARTESIAN_POINT('Ctrl Pts',(52.9004921312646,-4.81205812684748,333.974530565031));
#63135=CARTESIAN_POINT('Ctrl Pts',(52.8928540142355,-4.83844265646304,334.107296363423));
#63136=CARTESIAN_POINT('Ctrl Pts',(52.8852158972064,-4.85930351266948,334.240821210611));
#63137=CARTESIAN_POINT('Ctrl Pts',(52.8775694218147,-4.88018719683203,334.374492173534));
#63138=CARTESIAN_POINT('Ctrl Pts',(52.8699229464229,-4.89553508175743,334.508923443894));
#63139=CARTESIAN_POINT('Ctrl Pts',(52.8622764710312,-4.90532067276581,334.643612346122));
#63140=CARTESIAN_POINT('Ctrl Pts',(52.8554567728702,-4.91404819408577,334.763737974177));
#63141=CARTESIAN_POINT('Ctrl Pts',(52.8486370747092,-4.91835196711398,334.884068288334));
#63142=CARTESIAN_POINT('Ctrl Pts',(52.8418173765482,-4.9182481654623,335.0042479909));
#63143=CARTESIAN_POINT('',(51.0918173764711,-4.91824913722187,334.99708680308));
#63144=CARTESIAN_POINT('Ctrl Pts',(52.8418173765087,-4.9182481654617,335.004247991597));
#63145=CARTESIAN_POINT('Ctrl Pts',(52.8301934007741,-4.91807123855823,335.209090773998));
#63146=CARTESIAN_POINT('Ctrl Pts',(52.8185694250394,-4.90509378189171,335.41340122439));
#63147=CARTESIAN_POINT('Ctrl Pts',(52.8069454493047,-4.87953275582671,335.615908391982));
#63148=CARTESIAN_POINT('Ctrl Pts',(52.801421132238,-4.86738482849455,335.712150317087));
#63149=CARTESIAN_POINT('Ctrl Pts',(52.7958968151712,-4.85239533518121,335.807985504501));
#63150=CARTESIAN_POINT('Ctrl Pts',(52.7903724981044,-4.83459084839709,335.903279796683));
#63151=CARTESIAN_POINT('Ctrl Pts',(52.7825974193259,-4.80953231434074,336.037399656186));
#63152=CARTESIAN_POINT('Ctrl Pts',(52.7748223405475,-4.77884888101143,336.170687910591));
#63153=CARTESIAN_POINT('Ctrl Pts',(52.7670472617691,-4.74260715552524,336.302635954847));
#63154=CARTESIAN_POINT('Ctrl Pts',(52.7592817507201,-4.70641002778952,336.434421628634));
#63155=CARTESIAN_POINT('Ctrl Pts',(52.7515162396711,-4.66466831973847,336.564870000422));
#63156=CARTESIAN_POINT('Ctrl Pts',(52.743750728622,-4.6174999601803,336.693480788269));
#63157=CARTESIAN_POINT('Ctrl Pts',(52.7359929170998,-4.57037836818793,336.821964058144));
#63158=CARTESIAN_POINT('Ctrl Pts',(52.7282351055777,-4.51784096598995,336.948613005293));
#63159=CARTESIAN_POINT('Ctrl Pts',(52.7204772940555,-4.46005588579636,337.072941040665));
#63160=CARTESIAN_POINT('Ctrl Pts',(52.7127253205324,-4.40231429070805,337.197175515248));
#63161=CARTESIAN_POINT('Ctrl Pts',(52.7049733470094,-4.33933304208548,337.319092201465));
#63162=CARTESIAN_POINT('Ctrl Pts',(52.6972213734864,-4.27132878681837,337.438223422371));
#63163=CARTESIAN_POINT('Ctrl Pts',(52.6894726829288,-4.20335333139382,337.557304191134));
#63164=CARTESIAN_POINT('Ctrl Pts',(52.6817239923712,-4.13035929364046,337.673601502065));
#63165=CARTESIAN_POINT('Ctrl Pts',(52.6739753018135,-4.05260966892441,337.786671479353));
#63166=CARTESIAN_POINT('Ctrl Pts',(52.6662282234357,-3.97487622066722,337.899717931488));
#63167=CARTESIAN_POINT('Ctrl Pts',(52.6584811450579,-3.89238937484226,338.009538063712));
#63168=CARTESIAN_POINT('Ctrl Pts',(52.65073406668,-3.80545571651025,338.115716587268));
#63169=CARTESIAN_POINT('Ctrl Pts',(52.6429869233742,-3.71852132959033,338.221896000703));
#63170=CARTESIAN_POINT('Ctrl Pts',(52.6352397800684,-3.62714030344766,338.32443344216));
#63171=CARTESIAN_POINT('Ctrl Pts',(52.6274926367626,-3.53165955001809,338.42294666702));
#63172=CARTESIAN_POINT('Ctrl Pts',(52.6197437517345,-3.43615733048816,338.521482039745));
#63173=CARTESIAN_POINT('Ctrl Pts',(52.6119948667064,-3.33655382156292,338.615991114941));
#63174=CARTESIAN_POINT('Ctrl Pts',(52.6042459816783,-3.23323253375071,338.706128768027));
#63175=CARTESIAN_POINT('Ctrl Pts',(52.5964888719036,-3.12980157965603,338.796362094149));
#63176=CARTESIAN_POINT('Ctrl Pts',(52.5887317621288,-3.02264525899864,338.882214472215));
#63177=CARTESIAN_POINT('Ctrl Pts',(52.5809746523541,-2.91218031503351,338.963380990421));
#63178=CARTESIAN_POINT('Ctrl Pts',(52.5732133974279,-2.80165634213445,339.044590881419));
#63179=CARTESIAN_POINT('Ctrl Pts',(52.5654521425018,-2.68782054721736,339.121109705219));
#63180=CARTESIAN_POINT('Ctrl Pts',(52.5576908875756,-2.57111750366757,339.192676692142));
#63181=CARTESIAN_POINT('Ctrl Pts',(52.5499172171709,-2.45422777328145,339.264358162922));
#63182=CARTESIAN_POINT('Ctrl Pts',(52.5421435467662,-2.33446197040156,339.331071777361));
#63183=CARTESIAN_POINT('Ctrl Pts',(52.5343698763616,-2.21228882774224,339.392603010192));
#63184=CARTESIAN_POINT('Ctrl Pts',(52.5269580721845,-2.09580287426769,339.451269949331));
#63185=CARTESIAN_POINT('Ctrl Pts',(52.5195462680075,-1.97712892258029,339.505226009569));
#63186=CARTESIAN_POINT('Ctrl Pts',(52.5121344638305,-1.85668726517371,339.554327114058));
#63187=CARTESIAN_POINT('Ctrl Pts',(52.5043593850521,-1.73034240335963,339.605834809942));
#63188=CARTESIAN_POINT('Ctrl Pts',(52.4965843062737,-1.60165290026027,339.652162378791));
#63189=CARTESIAN_POINT('Ctrl Pts',(52.4888092274952,-1.4710824976472,339.69309059657));
#63190=CARTESIAN_POINT('Ctrl Pts',(52.4810437164462,-1.34067277022698,339.733968449572));
#63191=CARTESIAN_POINT('Ctrl Pts',(52.4732782053972,-1.20838711803129,339.769460055852));
#63192=CARTESIAN_POINT('Ctrl Pts',(52.4655126943482,-1.07471005686374,339.799393852996));
#63193=CARTESIAN_POINT('Ctrl Pts',(52.457754882826,-0.941165536891718,339.829297970693));
#63194=CARTESIAN_POINT('Ctrl Pts',(52.4499970713038,-0.806232732373306,
339.853655160765));
#63195=CARTESIAN_POINT('Ctrl Pts',(52.4422392597816,-0.670411812406666,
339.872343487921));
#63196=CARTESIAN_POINT('Ctrl Pts',(52.4344872862586,-0.53469310198943,339.891017751518));
#63197=CARTESIAN_POINT('Ctrl Pts',(52.4267353127356,-0.39808799207893,339.904031590395));
#63198=CARTESIAN_POINT('Ctrl Pts',(52.4189833392126,-0.261107002257901,
339.911314100714));
#63199=CARTESIAN_POINT('Ctrl Pts',(52.411234648655,-0.124184023967295,339.918593526886));
#63200=CARTESIAN_POINT('Ctrl Pts',(52.4034859580974,0.0131141281146278,
339.920146431363));
#63201=CARTESIAN_POINT('Ctrl Pts',(52.3957372675398,0.150271867464594,339.915953765888));
#63202=CARTESIAN_POINT('Ctrl Pts',(52.387990189162,0.28740107000123,339.911761972732));
#63203=CARTESIAN_POINT('Ctrl Pts',(52.3802431107841,0.424389527468195,339.901826999323));
#63204=CARTESIAN_POINT('Ctrl Pts',(52.3724960324063,0.560722103922002,339.886181923002));
#63205=CARTESIAN_POINT('Ctrl Pts',(52.3647488891005,0.697055822974018,339.870536715561));
#63206=CARTESIAN_POINT('Ctrl Pts',(52.3570017457947,0.832733261723166,339.849181354318));
#63207=CARTESIAN_POINT('Ctrl Pts',(52.3492546024889,0.967245248560456,339.822200710426));
#63208=CARTESIAN_POINT('Ctrl Pts',(52.3415057174608,1.10178747654825,339.795214000713));
#63209=CARTESIAN_POINT('Ctrl Pts',(52.3337568324328,1.23516334807102,339.762599568629));
#63210=CARTESIAN_POINT('Ctrl Pts',(52.3260079474047,1.36687510096273,339.724493149627));
#63211=CARTESIAN_POINT('Ctrl Pts',(52.31825083763,1.49872665406979,339.686346284078));
#63212=CARTESIAN_POINT('Ctrl Pts',(52.3104937278552,1.62891018410178,339.642695895937));
#63213=CARTESIAN_POINT('Ctrl Pts',(52.3027366180805,1.75694376052957,339.593727428226));
#63214=CARTESIAN_POINT('Ctrl Pts',(52.2949753631543,1.88504575400688,339.544732793331));
#63215=CARTESIAN_POINT('Ctrl Pts',(52.2872141082282,2.01099514592363,339.490414571013));
#63216=CARTESIAN_POINT('Ctrl Pts',(52.279452853302,2.13433206532665,339.431005495079));
#63217=CARTESIAN_POINT('Ctrl Pts',(52.2716791828974,2.25786628360531,339.371501383985));
#63218=CARTESIAN_POINT('Ctrl Pts',(52.2639055124927,2.37877933335822,339.306890330051));
#63219=CARTESIAN_POINT('Ctrl Pts',(52.2561318420881,2.49663715754374,339.237450408686));
#63220=CARTESIAN_POINT('Ctrl Pts',(52.2487200379109,2.60900867165918,339.171242932366));
#63221=CARTESIAN_POINT('Ctrl Pts',(52.2413082337338,2.71860275858495,339.100646194786));
#63222=CARTESIAN_POINT('Ctrl Pts',(52.2338964295567,2.82507081664059,339.025935660622));
#63223=CARTESIAN_POINT('Ctrl Pts',(52.2261213507782,2.93675719137287,338.947563340627));
#63224=CARTESIAN_POINT('Ctrl Pts',(52.2183462719998,3.0453563067021,338.86441609778));
#63225=CARTESIAN_POINT('Ctrl Pts',(52.2105711932214,3.15043285518016,338.776765267726));
#63226=CARTESIAN_POINT('Ctrl Pts',(52.2028056821724,3.25538010027588,338.689222297599));
#63227=CARTESIAN_POINT('Ctrl Pts',(52.1950401711233,3.35681310612936,338.597187015143));
#63228=CARTESIAN_POINT('Ctrl Pts',(52.1872746600743,3.45432540294311,338.500974017767));
#63229=CARTESIAN_POINT('Ctrl Pts',(52.1795168485521,3.5517410160306,338.404856415859));
#63230=CARTESIAN_POINT('Ctrl Pts',(52.1717590370299,3.64524337976807,338.304569615038));
#63231=CARTESIAN_POINT('Ctrl Pts',(52.1640012255077,3.73445928596813,338.200468231985));
#63232=CARTESIAN_POINT('Ctrl Pts',(52.1562492519847,3.82360805436958,338.096445188525));
#63233=CARTESIAN_POINT('Ctrl Pts',(52.1484972784616,3.90847653249157,337.988613572209));
#63234=CARTESIAN_POINT('Ctrl Pts',(52.1407453049386,3.98872882434416,337.877364319711));
#63235=CARTESIAN_POINT('Ctrl Pts',(52.132996614381,4.06894712930346,337.766162181338));
#63236=CARTESIAN_POINT('Ctrl Pts',(52.1252479238234,4.14455290806584,337.651545601842));
#63237=CARTESIAN_POINT('Ctrl Pts',(52.1174992332658,4.21525112909324,337.533937840828));
#63238=CARTESIAN_POINT('Ctrl Pts',(52.1097521548879,4.28593464076531,337.41635454909));
#63239=CARTESIAN_POINT('Ctrl Pts',(52.1020050765101,4.35171242440333,337.295781648504));
#63240=CARTESIAN_POINT('Ctrl Pts',(52.0942579981323,4.41233352583294,337.172670227925));
#63241=CARTESIAN_POINT('Ctrl Pts',(52.0865108548265,4.47295513532572,337.049557775553));
#63242=CARTESIAN_POINT('Ctrl Pts',(52.0787637115206,4.52841980373728,336.923907111419));
#63243=CARTESIAN_POINT('Ctrl Pts',(52.0710165682148,4.5785233590557,336.796192337441));
#63244=CARTESIAN_POINT('Ctrl Pts',(52.0632676831867,4.62863817871705,336.66844885047));
#63245=CARTESIAN_POINT('Ctrl Pts',(52.0555187981587,4.6733893441656,336.538640694041));
#63246=CARTESIAN_POINT('Ctrl Pts',(52.0477699131306,4.71262163057042,336.407259901219));
#63247=CARTESIAN_POINT('Ctrl Pts',(52.0400128033558,4.7518955585294,336.275739659467));
#63248=CARTESIAN_POINT('Ctrl Pts',(52.0322556935811,4.78563879393154,336.142643822037));
#63249=CARTESIAN_POINT('Ctrl Pts',(52.0244985838063,4.81374647950684,336.008478008454));
#63250=CARTESIAN_POINT('Ctrl Pts',(52.0167373288802,4.8418691849306,335.87424050095));
#63251=CARTESIAN_POINT('Ctrl Pts',(52.008976073954,4.86435027589497,335.738932263399));
#63252=CARTESIAN_POINT('Ctrl Pts',(52.0012148190278,4.88113660066499,335.603065956715));
#63253=CARTESIAN_POINT('Ctrl Pts',(51.9934411486231,4.89794977808398,335.466982308219));
#63254=CARTESIAN_POINT('Ctrl Pts',(51.9856674782185,4.9090499536254,335.33033919645));
#63255=CARTESIAN_POINT('Ctrl Pts',(51.9778938078138,4.91443607366073,335.193652111794));
#63256=CARTESIAN_POINT('Ctrl Pts',(51.9704820036368,4.91957146851257,335.063327843813));
#63257=CARTESIAN_POINT('Ctrl Pts',(51.9630701994597,4.91951281470945,334.932963892487));
#63258=CARTESIAN_POINT('Ctrl Pts',(51.9556583952827,4.91430310800094,334.803002474147));
#63259=CARTESIAN_POINT('Ctrl Pts',(51.9478833165042,4.90883805804771,334.666671259558));
#63260=CARTESIAN_POINT('Ctrl Pts',(51.9401082377258,4.89768698038941,334.530352202525));
#63261=CARTESIAN_POINT('Ctrl Pts',(51.9323331589474,4.88084247712137,334.394558197654));
#63262=CARTESIAN_POINT('Ctrl Pts',(51.9245676478984,4.86401870208698,334.258931295952));
#63263=CARTESIAN_POINT('Ctrl Pts',(51.9168021368494,4.84151548927516,334.123828545031));
#63264=CARTESIAN_POINT('Ctrl Pts',(51.9090366258004,4.81337742622822,333.989762000726));
#63265=CARTESIAN_POINT('Ctrl Pts',(51.9012788142782,4.78526726215274,333.855828383791));
#63266=CARTESIAN_POINT('Ctrl Pts',(51.893521002756,4.75153344599989,333.722929308959));
#63267=CARTESIAN_POINT('Ctrl Pts',(51.8857631912338,4.71227221813807,333.591570518391));
#63268=CARTESIAN_POINT('Ctrl Pts',(51.8780112177108,4.67304053559524,333.46031057948));
#63269=CARTESIAN_POINT('Ctrl Pts',(51.8702592441877,4.62828983221271,333.330588990672));
#63270=CARTESIAN_POINT('Ctrl Pts',(51.8625072706647,4.57816708238549,333.202899772338));
#63271=CARTESIAN_POINT('Ctrl Pts',(51.8547585801071,4.52806555957258,333.075264630464));
#63272=CARTESIAN_POINT('Ctrl Pts',(51.8470098895495,4.47259665778465,332.949660510262));
#63273=CARTESIAN_POINT('Ctrl Pts',(51.8392611989919,4.41195664655668,332.826564560102));
#63274=CARTESIAN_POINT('Ctrl Pts',(51.8315141206141,4.35132925198956,332.703494221083));
#63275=CARTESIAN_POINT('Ctrl Pts',(51.8237670422362,4.28553306063243,332.582931364536));
#63276=CARTESIAN_POINT('Ctrl Pts',(51.8160199638584,4.21481159702181,332.465331133242));
#63277=CARTESIAN_POINT('Ctrl Pts',(51.8082728205526,4.1440895406972,332.347729916345));
#63278=CARTESIAN_POINT('Ctrl Pts',(51.8005256772468,4.06844233122693,332.233091709194));
#63279=CARTESIAN_POINT('Ctrl Pts',(51.792778533941,3.98815816183793,332.121844768143));
#63280=CARTESIAN_POINT('Ctrl Pts',(51.7850296489129,3.90785594286322,332.010572816418));
#63281=CARTESIAN_POINT('Ctrl Pts',(51.7772807638848,3.82291491823161,331.902693964833));
#63282=CARTESIAN_POINT('Ctrl Pts',(51.7695318788567,3.73366484798352,331.798605012587));
#63283=CARTESIAN_POINT('Ctrl Pts',(51.761774769082,3.64432004678869,331.694405579252));
#63284=CARTESIAN_POINT('Ctrl Pts',(51.7540176593073,3.55065731848177,331.594004378051));
#63285=CARTESIAN_POINT('Ctrl Pts',(51.7462605495326,3.45304510502089,331.497763205437));
#63286=CARTESIAN_POINT('Ctrl Pts',(51.7384992946064,3.35538073071417,331.401470604617));
#63287=CARTESIAN_POINT('Ctrl Pts',(51.7307380396802,3.25376295536853,331.309342724288));
#63288=CARTESIAN_POINT('Ctrl Pts',(51.722976784754,3.14859412302986,331.221701691115));
#63289=CARTESIAN_POINT('Ctrl Pts',(51.7152031143494,3.04325705483388,331.133920460851));
#63290=CARTESIAN_POINT('Ctrl Pts',(51.7074294439447,2.9343578889078,331.050640658068));
#63291=CARTESIAN_POINT('Ctrl Pts',(51.69965577354,2.82232954193554,330.972142130211));
#63292=CARTESIAN_POINT('Ctrl Pts',(51.692243969363,2.71551614146754,330.897297727712));
#63293=CARTESIAN_POINT('Ctrl Pts',(51.6848321651859,2.60585857266585,330.826799636602));
#63294=CARTESIAN_POINT('Ctrl Pts',(51.6774203610088,2.49375197214532,330.760851009469));
#63295=CARTESIAN_POINT('Ctrl Pts',(51.6696452822304,2.37615069318461,330.691670043669));
#63296=CARTESIAN_POINT('Ctrl Pts',(51.661870203452,2.25548260191611,330.627277159023));
#63297=CARTESIAN_POINT('Ctrl Pts',(51.6540951246735,2.13217499892654,330.567956133289));
#63298=CARTESIAN_POINT('Ctrl Pts',(51.6463296136245,2.00901913379259,330.508708105853));
#63299=CARTESIAN_POINT('Ctrl Pts',(51.6385641025755,1.88323056856601,330.454519686874));
#63300=CARTESIAN_POINT('Ctrl Pts',(51.6307985915265,1.75526403079943,330.40563048453));
#63301=CARTESIAN_POINT('Ctrl Pts',(51.6230407800043,1.6274243722277,330.356789755972));
#63302=CARTESIAN_POINT('Ctrl Pts',(51.6152829684821,1.49741140135767,330.313237926515));
#63303=CARTESIAN_POINT('Ctrl Pts',(51.6075251569599,1.36570248874796,330.275167751684));
#63304=CARTESIAN_POINT('Ctrl Pts',(51.5997731834369,1.2340926912719,330.237126225867));
#63305=CARTESIAN_POINT('Ctrl Pts',(51.5920212099139,1.10078986635988,330.204558251928));
#63306=CARTESIAN_POINT('Ctrl Pts',(51.5842692363909,0.966288982558887,330.177607578734));
#63307=CARTESIAN_POINT('Ctrl Pts',(51.5765205458332,0.831845059961858,330.150668319165));
#63308=CARTESIAN_POINT('Ctrl Pts',(51.5687718552756,0.696204470074705,330.129341705451));
#63309=CARTESIAN_POINT('Ctrl Pts',(51.561023164718,0.559874669850121,330.113720902715));
#63310=CARTESIAN_POINT('Ctrl Pts',(51.5532760863402,0.42357323417903,330.098103350018));
#63311=CARTESIAN_POINT('Ctrl Pts',(51.5455290079624,0.286583261484846,330.088189291458));
#63312=CARTESIAN_POINT('Ctrl Pts',(51.5377819295845,0.149419276142205,330.084020245931));
#63313=CARTESIAN_POINT('Ctrl Pts',(51.5300347862787,0.0122541412333472,
330.079851165464));
#63314=CARTESIAN_POINT('Ctrl Pts',(51.5222876429728,-0.12508461853898,330.081427205941));
#63315=CARTESIAN_POINT('Ctrl Pts',(51.514540499667,-0.262080915379637,330.088737773617));
#63316=CARTESIAN_POINT('Ctrl Pts',(51.5067916146389,-0.399108011896339,
330.096049984864));
#63317=CARTESIAN_POINT('Ctrl Pts',(51.4990427296108,-0.535792102031358,
330.109099267934));
#63318=CARTESIAN_POINT('Ctrl Pts',(51.4912938445827,-0.671621056794774,
330.12782305139));
#63319=CARTESIAN_POINT('Ctrl Pts',(51.483536734808,-0.807594181814151,330.146566708462));
#63320=CARTESIAN_POINT('Ctrl Pts',(51.4757796250333,-0.942709970522598,
330.170996843913));
#63321=CARTESIAN_POINT('Ctrl Pts',(51.4680225152585,-1.07646479548064,330.200999415858));
#63322=CARTESIAN_POINT('Ctrl Pts',(51.4602612603324,-1.21029109474039,330.231018020219));
#63323=CARTESIAN_POINT('Ctrl Pts',(51.4525000054062,-1.3427546038373,330.266614893085));
#63324=CARTESIAN_POINT('Ctrl Pts',(51.44473875048,-1.47336670813691,330.307626015986));
#63325=CARTESIAN_POINT('Ctrl Pts',(51.4369650800753,-1.60418774923711,330.348702743318));
#63326=CARTESIAN_POINT('Ctrl Pts',(51.4291914096707,-1.73315109940952,330.395210895327));
#63327=CARTESIAN_POINT('Ctrl Pts',(51.421417739266,-1.85978715290873,330.446937864648));
#63328=CARTESIAN_POINT('Ctrl Pts',(51.4140059350889,-1.9805282676512,330.496256931103));
#63329=CARTESIAN_POINT('Ctrl Pts',(51.4065941309118,-2.09915361910606,330.550319757871));
#63330=CARTESIAN_POINT('Ctrl Pts',(51.3991823267346,-2.21527854083245,330.608904003665));
#63331=CARTESIAN_POINT('Ctrl Pts',(51.3914072479562,-2.33709509089033,330.670359637859));
#63332=CARTESIAN_POINT('Ctrl Pts',(51.3836321691778,-2.45654486946993,330.736985325403));
#63333=CARTESIAN_POINT('Ctrl Pts',(51.3758570903994,-2.57315800493463,330.808575308545));
#63334=CARTESIAN_POINT('Ctrl Pts',(51.3680915793503,-2.68962764051227,330.880077195655));
#63335=CARTESIAN_POINT('Ctrl Pts',(51.3603260683013,-2.80326724848132,330.956531020895));
#63336=CARTESIAN_POINT('Ctrl Pts',(51.3525605572523,-2.91362925804211,331.037684059899));
#63337=CARTESIAN_POINT('Ctrl Pts',(51.3448027457301,-3.0238818433491,331.118756635428));
#63338=CARTESIAN_POINT('Ctrl Pts',(51.3370449342079,-3.13086298455721,331.204518922415));
#63339=CARTESIAN_POINT('Ctrl Pts',(51.3292871226857,-3.23415225683324,331.294673800848));
#63340=CARTESIAN_POINT('Ctrl Pts',(51.3215351491626,-3.33736380065632,331.384760834876));
#63341=CARTESIAN_POINT('Ctrl Pts',(51.3137831756397,-3.4368887122227,331.479233624788));
#63342=CARTESIAN_POINT('Ctrl Pts',(51.3060312021167,-3.53233825416323,331.577753731732));
#63343=CARTESIAN_POINT('Ctrl Pts',(51.298282511559,-3.62774737316614,331.676232115352));
#63344=CARTESIAN_POINT('Ctrl Pts',(51.2905338210014,-3.71908428386492,331.778754126752));
#63345=CARTESIAN_POINT('Ctrl Pts',(51.2827851304438,-3.80599602764457,331.884943451548));
#63346=CARTESIAN_POINT('Ctrl Pts',(51.275038052066,-3.89288968870991,331.991110682768));
#63347=CARTESIAN_POINT('Ctrl Pts',(51.2672909736881,-3.97535976676811,332.100943407404));
#63348=CARTESIAN_POINT('Ctrl Pts',(51.2595438953103,-4.05309290903067,332.214031419189));
#63349=CARTESIAN_POINT('Ctrl Pts',(51.2517967520045,-4.13082670277188,332.327120378761));
#63350=CARTESIAN_POINT('Ctrl Pts',(51.2440496086987,-4.20382326011985,332.443464357784));
#63351=CARTESIAN_POINT('Ctrl Pts',(51.2363024653929,-4.27181220486338,332.562623634134));
#63352=CARTESIAN_POINT('Ctrl Pts',(51.2285535803648,-4.33981643496509,332.68180970002));
#63353=CARTESIAN_POINT('Ctrl Pts',(51.2208046953367,-4.40281061854024,332.803811983279));
#63354=CARTESIAN_POINT('Ctrl Pts',(51.2130558103086,-4.46057023086444,332.928165962721));
#63355=CARTESIAN_POINT('Ctrl Pts',(51.2052987005339,-4.51839114983793,333.052651932762));
#63356=CARTESIAN_POINT('Ctrl Pts',(51.1975415907591,-4.57096623395574,333.179494230149));
#63357=CARTESIAN_POINT('Ctrl Pts',(51.1897844809844,-4.61811884176474,333.308207629218));
#63358=CARTESIAN_POINT('Ctrl Pts',(51.1820232260582,-4.66529664641974,333.436989808611));
#63359=CARTESIAN_POINT('Ctrl Pts',(51.1742619711321,-4.7070460821278,333.567644709851));
#63360=CARTESIAN_POINT('Ctrl Pts',(51.1665007162059,-4.74324065810402,333.699672686664));
#63361=CARTESIAN_POINT('Ctrl Pts',(51.1587270458012,-4.779493133606,333.831911865211));
#63362=CARTESIAN_POINT('Ctrl Pts',(51.1509533753965,-4.81017290506724,333.965528127372));
#63363=CARTESIAN_POINT('Ctrl Pts',(51.1431797049919,-4.83520462794207,334.100011517614));
#63364=CARTESIAN_POINT('Ctrl Pts',(51.1357679008148,-4.85907111809463,334.228234673684));
#63365=CARTESIAN_POINT('Ctrl Pts',(51.1283560966379,-4.8778035180788,334.35724576017));
#63366=CARTESIAN_POINT('Ctrl Pts',(51.1209442924608,-4.8913806343428,334.486600981228));
#63367=CARTESIAN_POINT('Ctrl Pts',(51.1112353204767,-4.90916575632966,334.656047743074));
#63368=CARTESIAN_POINT('Ctrl Pts',(51.1015263484927,-4.91814805570971,334.826434437093));
#63369=CARTESIAN_POINT('Ctrl Pts',(51.0918173765087,-4.91824913722148,334.997086802418));
#63370=CARTESIAN_POINT('',(49.3418173765595,-4.9182492637269,334.997308838587));
#63371=CARTESIAN_POINT('Ctrl Pts',(51.0918173764711,-4.91824913722187,334.99708680308));
#63372=CARTESIAN_POINT('Ctrl Pts',(51.0841469556418,-4.91832899506454,335.131908024081));
#63373=CARTESIAN_POINT('Ctrl Pts',(51.0764765348125,-4.91286100890517,335.266951588975));
#63374=CARTESIAN_POINT('Ctrl Pts',(51.0688061139833,-4.90181674892083,335.401715847956));
#63375=CARTESIAN_POINT('Ctrl Pts',(51.0611442022096,-4.89078474070522,335.536330608416));
#63376=CARTESIAN_POINT('Ctrl Pts',(51.053482290436,-4.87418879416588,335.670666282156));
#63377=CARTESIAN_POINT('Ctrl Pts',(51.0458203786623,-4.85205248533923,335.804219958726));
#63378=CARTESIAN_POINT('Ctrl Pts',(51.0381650213289,-4.82993511318494,335.937659385796));
#63379=CARTESIAN_POINT('Ctrl Pts',(51.0305096639954,-4.80228687237235,336.07031775213));
#63380=CARTESIAN_POINT('Ctrl Pts',(51.022854306662,-4.76918321498598,336.201696519258));
#63381=CARTESIAN_POINT('Ctrl Pts',(51.0152031031228,-4.73609751963295,336.333004000311));
#63382=CARTESIAN_POINT('Ctrl Pts',(51.0075518995837,-4.69756239229167,336.463032874332));
#63383=CARTESIAN_POINT('Ctrl Pts',(50.9999006960446,-4.65370443417213,336.591294473649));
#63384=CARTESIAN_POINT('Ctrl Pts',(50.992251590838,-4.60985850403989,336.719520897391));
#63385=CARTESIAN_POINT('Ctrl Pts',(50.9846024856314,-4.56069277513262,336.845980630099));
#63386=CARTESIAN_POINT('Ctrl Pts',(50.9769533804247,-4.50638366360705,336.97020032963));
#63387=CARTESIAN_POINT('Ctrl Pts',(50.9693046166191,-4.45207697604924,337.094414484889));
#63388=CARTESIAN_POINT('Ctrl Pts',(50.9616558528135,-4.39262752341957,337.216388437617));
#63389=CARTESIAN_POINT('Ctrl Pts',(50.9540070890078,-4.32825958614541,337.335669500901));
#63390=CARTESIAN_POINT('Ctrl Pts',(50.9463569101738,-4.26387974074317,337.454972631292));
#63391=CARTESIAN_POINT('Ctrl Pts',(50.9387067313398,-4.19457979238958,337.571581528133));
#63392=CARTESIAN_POINT('Ctrl Pts',(50.9310565525058,-4.12062935113851,337.685069238034));
#63393=CARTESIAN_POINT('Ctrl Pts',(50.9233986125228,-4.04660388675388,337.798672081847));
#63394=CARTESIAN_POINT('Ctrl Pts',(50.9157406725398,-3.96791872714121,337.909147077951));
#63395=CARTESIAN_POINT('Ctrl Pts',(50.9080827325569,-3.8848862990819,338.016097065034));
#63396=CARTESIAN_POINT('Ctrl Pts',(50.9004207899194,-3.80181047160636,338.123102952771));
#63397=CARTESIAN_POINT('Ctrl Pts',(50.8927588472818,-3.71438311033859,338.226579856244));
#63398=CARTESIAN_POINT('Ctrl Pts',(50.8850969046443,-3.62295524746866,338.326165711046));
#63399=CARTESIAN_POINT('Ctrl Pts',(50.8774230661438,-3.53138543452352,338.425906181949));
#63400=CARTESIAN_POINT('Ctrl Pts',(50.8697492276433,-3.43580299719714,338.521743253069));
#63401=CARTESIAN_POINT('Ctrl Pts',(50.8620753891428,-3.33659440678278,338.613353127931));
#63402=CARTESIAN_POINT('Ctrl Pts',(50.8556190121575,-3.25312535021489,338.690429012137));
#63403=CARTESIAN_POINT('Ctrl Pts',(50.8491626351722,-3.1670901464203,338.764513228407));
#63404=CARTESIAN_POINT('Ctrl Pts',(50.8427062581869,-3.07873491637792,338.835436660561));
#63405=CARTESIAN_POINT('Ctrl Pts',(50.8349311794085,-2.97233331132417,338.920846058663));
#63406=CARTESIAN_POINT('Ctrl Pts',(50.8271561006301,-2.86220677301116,339.001959420094));
#63407=CARTESIAN_POINT('Ctrl Pts',(50.8193810218516,-2.74873723671036,339.078434340041));
#63408=CARTESIAN_POINT('Ctrl Pts',(50.8116155108026,-2.63540733189781,339.15481515273));
#63409=CARTESIAN_POINT('Ctrl Pts',(50.8038499997536,-2.51874293535591,339.226568664648));
#63410=CARTESIAN_POINT('Ctrl Pts',(50.7960844887046,-2.39915948944647,339.293392226049));
#63411=CARTESIAN_POINT('Ctrl Pts',(50.7883266771824,-2.27969461087205,339.360149531694));
#63412=CARTESIAN_POINT('Ctrl Pts',(50.7805688656602,-2.15731678165935,339.421986424894));
#63413=CARTESIAN_POINT('Ctrl Pts',(50.772811054138,-2.03247060399064,339.478643355573));
#63414=CARTESIAN_POINT('Ctrl Pts',(50.765059080615,-1.9077183770299,339.535257650114));
#63415=CARTESIAN_POINT('Ctrl Pts',(50.7573071070921,-1.78050185340068,339.586699580206));
#63416=CARTESIAN_POINT('Ctrl Pts',(50.7495551335691,-1.65129011324519,339.632755554138));
#63417=CARTESIAN_POINT('Ctrl Pts',(50.7418064430115,-1.52213309433811,339.678792023338));
#63418=CARTESIAN_POINT('Ctrl Pts',(50.7340577524539,-1.39098290691982,339.719446942075));
#63419=CARTESIAN_POINT('Ctrl Pts',(50.7263090618962,-1.2583282801843,339.754554974105));
#63420=CARTESIAN_POINT('Ctrl Pts',(50.7185619835184,-1.12570125335173,339.789655701616));
#63421=CARTESIAN_POINT('Ctrl Pts',(50.7108149051406,-0.991570787430775,
339.819211738016));
#63422=CARTESIAN_POINT('Ctrl Pts',(50.7030678267627,-0.856440049436659,
339.843107835287));
#63423=CARTESIAN_POINT('Ctrl Pts',(50.6953206834569,-0.721308178916805,
339.867004132831));
#63424=CARTESIAN_POINT('Ctrl Pts',(50.6875735401511,-0.585176404505199,
339.885240328567));
#63425=CARTESIAN_POINT('Ctrl Pts',(50.6798263968453,-0.44855695174069,339.897752517589));
#63426=CARTESIAN_POINT('Ctrl Pts',(50.6720775118172,-0.311906784022686,
339.910267519616));
#63427=CARTESIAN_POINT('Ctrl Pts',(50.6643286267892,-0.174769108948748,
339.917055918543));
#63428=CARTESIAN_POINT('Ctrl Pts',(50.6565797417611,-0.0376597265694707,
339.918105814996));
#63429=CARTESIAN_POINT('Ctrl Pts',(50.6488226319864,0.0995951851247759,
339.91915682582));
#63430=CARTESIAN_POINT('Ctrl Pts',(50.6410655222116,0.236821352656112,339.914457164016));
#63431=CARTESIAN_POINT('Ctrl Pts',(50.6333084124369,0.373503969883856,339.904047088577));
#63432=CARTESIAN_POINT('Ctrl Pts',(50.6255471575107,0.510259625931983,339.893631450327));
#63433=CARTESIAN_POINT('Ctrl Pts',(50.6177859025845,0.646470764952424,339.877499364075));
#63434=CARTESIAN_POINT('Ctrl Pts',(50.6100246476584,0.781630233297696,339.855742707444));
#63435=CARTESIAN_POINT('Ctrl Pts',(50.6022509772537,0.917005912743952,339.833951247253));
#63436=CARTESIAN_POINT('Ctrl Pts',(50.5944773068491,1.05132617655124,339.806517315313));
#63437=CARTESIAN_POINT('Ctrl Pts',(50.5867036364444,1.18409567793988,339.773583610662));
#63438=CARTESIAN_POINT('Ctrl Pts',(50.5792918322673,1.31068472709719,339.742182977887));
#63439=CARTESIAN_POINT('Ctrl Pts',(50.5718800280901,1.43586386437549,339.705783158708));
#63440=CARTESIAN_POINT('Ctrl Pts',(50.564468223913,1.55922039229397,339.66454872745));
#63441=CARTESIAN_POINT('Ctrl Pts',(50.5566931451346,1.68862299110521,339.621293273885));
#63442=CARTESIAN_POINT('Ctrl Pts',(50.5489180663561,1.81642873615065,339.572580612525));
#63443=CARTESIAN_POINT('Ctrl Pts',(50.5411429875777,1.94214300482772,339.518546625996));
#63444=CARTESIAN_POINT('Ctrl Pts',(50.5333774765287,2.06770257409373,339.464579131728));
#63445=CARTESIAN_POINT('Ctrl Pts',(50.5256119654797,2.1911754322309,339.405303494265));
#63446=CARTESIAN_POINT('Ctrl Pts',(50.5178464544306,2.31208225490912,339.340905286808));
#63447=CARTESIAN_POINT('Ctrl Pts',(50.5100886429084,2.43286919812064,339.276570930361));
#63448=CARTESIAN_POINT('Ctrl Pts',(50.5023308313862,2.5510948262701,339.20712429407));
#63449=CARTESIAN_POINT('Ctrl Pts',(50.494573019864,2.66630027840952,339.132798795956));
#63450=CARTESIAN_POINT('Ctrl Pts',(50.486821046341,2.78141903479267,339.058529230136));
#63451=CARTESIAN_POINT('Ctrl Pts',(50.479069072818,2.8935218118911,338.979388321481));
#63452=CARTESIAN_POINT('Ctrl Pts',(50.471317099295,3.00217514969789,338.895654942758));
#63453=CARTESIAN_POINT('Ctrl Pts',(50.4635684087374,3.11078247275177,338.811957025171));
#63454=CARTESIAN_POINT('Ctrl Pts',(50.4558197181798,3.21594295306105,338.723670743912));
#63455=CARTESIAN_POINT('Ctrl Pts',(50.4480710276222,3.31725307643952,338.631117608857));
#63456=CARTESIAN_POINT('Ctrl Pts',(50.4403239492443,3.41854212140067,338.538583730255));
#63457=CARTESIAN_POINT('Ctrl Pts',(50.4325768708665,3.51598211447419,338.441785027135));
#63458=CARTESIAN_POINT('Ctrl Pts',(50.4248297924887,3.60920384859934,338.34108225606));
#63459=CARTESIAN_POINT('Ctrl Pts',(50.4170826491828,3.70242636401235,338.240378640998));
#63460=CARTESIAN_POINT('Ctrl Pts',(50.409335505877,3.79143028443259,338.135771179556));
#63461=CARTESIAN_POINT('Ctrl Pts',(50.4015883625712,3.87588467622995,338.027656030507));
#63462=CARTESIAN_POINT('Ctrl Pts',(50.3938394775432,3.96035805516715,337.919516574878));
#63463=CARTESIAN_POINT('Ctrl Pts',(50.3860905925151,4.04027962958914,337.807868170382));
#63464=CARTESIAN_POINT('Ctrl Pts',(50.378341707487,4.1153602640547,337.693138124854));
#63465=CARTESIAN_POINT('Ctrl Pts',(50.3705845977123,4.19052058988183,337.578286303668));
#63466=CARTESIAN_POINT('Ctrl Pts',(50.3628274879376,4.26082949729539,337.460346635131));
#63467=CARTESIAN_POINT('Ctrl Pts',(50.3550703781628,4.32604224979836,337.339773817158));
#63468=CARTESIAN_POINT('Ctrl Pts',(50.3473091232367,4.39128984991135,337.219136568927));
#63469=CARTESIAN_POINT('Ctrl Pts',(50.3395478683104,4.45143569753717,337.095863718657));
#63470=CARTESIAN_POINT('Ctrl Pts',(50.3317866133843,4.50628260458853,336.970431462925));
#63471=CARTESIAN_POINT('Ctrl Pts',(50.3240129429796,4.5612172488165,336.844798556461));
#63472=CARTESIAN_POINT('Ctrl Pts',(50.3162392725749,4.61083587221203,336.716999706297));
#63473=CARTESIAN_POINT('Ctrl Pts',(50.3084656021702,4.65499041287568,336.587528682744));
#63474=CARTESIAN_POINT('Ctrl Pts',(50.3010537979931,4.69708954904838,336.464084566487));
#63475=CARTESIAN_POINT('Ctrl Pts',(50.2936419938161,4.7342217785034,336.339120728592));
#63476=CARTESIAN_POINT('Ctrl Pts',(50.286230189639,4.76630216101283,336.213073275785));
#63477=CARTESIAN_POINT('Ctrl Pts',(50.2784551108606,4.79995489863162,336.08084786184));
#63478=CARTESIAN_POINT('Ctrl Pts',(50.2706800320822,4.8281544045909,335.947012068022));
#63479=CARTESIAN_POINT('Ctrl Pts',(50.2629049533037,4.85074727681879,335.812055366915));
#63480=CARTESIAN_POINT('Ctrl Pts',(50.2551394422547,4.87331234707906,335.67726473862));
#63481=CARTESIAN_POINT('Ctrl Pts',(50.2473739312057,4.89028444735542,335.541356329369));
#63482=CARTESIAN_POINT('Ctrl Pts',(50.2396084201567,4.90156024021243,335.404833637521));
#63483=CARTESIAN_POINT('Ctrl Pts',(50.2318506086345,4.91282485308801,335.26844630832));
#63484=CARTESIAN_POINT('Ctrl Pts',(50.2240927971123,4.91840436622867,335.131446295632));
#63485=CARTESIAN_POINT('Ctrl Pts',(50.2163349855901,4.91824674983992,334.994345781301));
#63486=CARTESIAN_POINT('Ctrl Pts',(50.2085830120671,4.91808925206249,334.857348439456));
#63487=CARTESIAN_POINT('Ctrl Pts',(50.2008310385441,4.91220321872094,334.720251135808));
#63488=CARTESIAN_POINT('Ctrl Pts',(50.1930790650211,4.90058858979415,334.583569290182));
#63489=CARTESIAN_POINT('Ctrl Pts',(50.1853303744635,4.88897887966959,334.446945329399));
#63490=CARTESIAN_POINT('Ctrl Pts',(50.1775816839058,4.87164543225606,334.310736865351));
#63491=CARTESIAN_POINT('Ctrl Pts',(50.1698329933482,4.8486402473879,334.17545720917));
#63492=CARTESIAN_POINT('Ctrl Pts',(50.1620859149704,4.8256398489406,334.040205699051));
#63493=CARTESIAN_POINT('Ctrl Pts',(50.1543388365926,4.79697012573504,333.905882997518));
#63494=CARTESIAN_POINT('Ctrl Pts',(50.1465917582148,4.76273464653511,333.77299480474));
#63495=CARTESIAN_POINT('Ctrl Pts',(50.138844614909,4.72849888040889,333.640105498232));
#63496=CARTESIAN_POINT('Ctrl Pts',(50.1310974716031,4.68869736276388,333.508651102975));
#63497=CARTESIAN_POINT('Ctrl Pts',(50.1233503282973,4.64348414478651,333.37912429236));
#63498=CARTESIAN_POINT('Ctrl Pts',(50.1156014432692,4.59826076191777,333.249568361369));
#63499=CARTESIAN_POINT('Ctrl Pts',(50.1078525582411,4.54762338648169,333.121941246328));
#63500=CARTESIAN_POINT('Ctrl Pts',(50.100103673213,4.49177488297321,332.996717328186));
#63501=CARTESIAN_POINT('Ctrl Pts',(50.0923465634383,4.43586710128616,332.871360496083));
#63502=CARTESIAN_POINT('Ctrl Pts',(50.0845894536636,4.37473730200621,332.748412313842));
#63503=CARTESIAN_POINT('Ctrl Pts',(50.0768323438888,4.308635409351,332.628324648737));
#63504=CARTESIAN_POINT('Ctrl Pts',(50.0690710889627,4.24249819395783,332.508172812624));
#63505=CARTESIAN_POINT('Ctrl Pts',(50.0613098340365,4.17138379357379,332.390884873525));
#63506=CARTESIAN_POINT('Ctrl Pts',(50.0535485791103,4.09558594226896,332.2768843484));
#63507=CARTESIAN_POINT('Ctrl Pts',(50.0457749087057,4.0196668391046,332.162701459588));
#63508=CARTESIAN_POINT('Ctrl Pts',(50.038001238301,3.93904954376794,332.051816809687));
#63509=CARTESIAN_POINT('Ctrl Pts',(50.0302275678964,3.85406915345952,331.944622114557));
#63510=CARTESIAN_POINT('Ctrl Pts',(50.0228157637193,3.77304462076529,331.842417358276));
#63511=CARTESIAN_POINT('Ctrl Pts',(50.0154039595422,3.6880542434981,331.743566971237));
#63512=CARTESIAN_POINT('Ctrl Pts',(50.0079921553652,3.59941878707636,331.648378383865));
#63513=CARTESIAN_POINT('Ctrl Pts',(50.0002170765867,3.50643904290366,331.548524320274));
#63514=CARTESIAN_POINT('Ctrl Pts',(49.9924419978083,3.40915403938212,331.452384526571));
#63515=CARTESIAN_POINT('Ctrl Pts',(49.9846669190299,3.30789236978766,331.360352883534));
#63516=CARTESIAN_POINT('Ctrl Pts',(49.9769014079809,3.20675530912421,331.268434491293));
#63517=CARTESIAN_POINT('Ctrl Pts',(49.9691358969318,3.10165160562392,331.180614451417));
#63518=CARTESIAN_POINT('Ctrl Pts',(49.9613703858828,2.99294873998521,331.097252134416));
#63519=CARTESIAN_POINT('Ctrl Pts',(49.9536125743606,2.88435365355442,331.013972471395));
#63520=CARTESIAN_POINT('Ctrl Pts',(49.9458547628384,2.77216681483068,330.935141971837));
#63521=CARTESIAN_POINT('Ctrl Pts',(49.9380969513163,2.6567907721474,330.861081559691));
#63522=CARTESIAN_POINT('Ctrl Pts',(49.9303449777932,2.54150155359495,330.787076880353));
#63523=CARTESIAN_POINT('Ctrl Pts',(49.9225930042703,2.4230282357331,330.717835353718));
#63524=CARTESIAN_POINT('Ctrl Pts',(49.9148410307473,2.30180421360705,330.653635953499));
#63525=CARTESIAN_POINT('Ctrl Pts',(49.9070923401896,2.18063152992625,330.589463741763));
#63526=CARTESIAN_POINT('Ctrl Pts',(49.899343649632,2.05671080363995,330.53032959195));
#63527=CARTESIAN_POINT('Ctrl Pts',(49.8915949590744,1.93050182912259,330.476467558395));
#63528=CARTESIAN_POINT('Ctrl Pts',(49.8838478806965,1.80431911343667,330.422616731286));
#63529=CARTESIAN_POINT('Ctrl Pts',(49.8761008023187,1.67584945577339,330.374035991936));
#63530=CARTESIAN_POINT('Ctrl Pts',(49.8683537239409,1.54557415719535,330.330911910543));
#63531=CARTESIAN_POINT('Ctrl Pts',(49.8606065806351,1.41529776678448,330.287787467728));
#63532=CARTESIAN_POINT('Ctrl Pts',(49.8528594373292,1.28321607634723,330.250119896918));
#63533=CARTESIAN_POINT('Ctrl Pts',(49.8451122940234,1.14982675138656,330.218046267027));
#63534=CARTESIAN_POINT('Ctrl Pts',(49.8373634089953,1.01640743767406,330.185965426303));
#63535=CARTESIAN_POINT('Ctrl Pts',(49.8296145239672,0.881680284410798,330.159481120417));
#63536=CARTESIAN_POINT('Ctrl Pts',(49.8218656389391,0.74615399027515,330.138679471039));
#63537=CARTESIAN_POINT('Ctrl Pts',(49.8141085291644,0.610483847130658,330.117855742576));
#63538=CARTESIAN_POINT('Ctrl Pts',(49.8063514193896,0.474013255682081,330.102726778761));
#63539=CARTESIAN_POINT('Ctrl Pts',(49.7985943096149,0.337257449096062,330.0933269443));
#63540=CARTESIAN_POINT('Ctrl Pts',(49.7908330546887,0.200428564579514,330.083922086868));
#63541=CARTESIAN_POINT('Ctrl Pts',(49.7830717997626,0.063314551771338,330.080252469483));
#63542=CARTESIAN_POINT('Ctrl Pts',(49.7753105448364,-0.0735694885215804,
330.082300274228));
#63543=CARTESIAN_POINT('Ctrl Pts',(49.7675368744317,-0.21067249866847,330.084351354793));
#63544=CARTESIAN_POINT('Ctrl Pts',(49.7597632040271,-0.347544410716231,
330.092138111715));
#63545=CARTESIAN_POINT('Ctrl Pts',(49.7519895336224,-0.483674482119245,
330.105590734537));
#63546=CARTESIAN_POINT('Ctrl Pts',(49.7445777294453,-0.613467665948094,
330.118417134531));
#63547=CARTESIAN_POINT('Ctrl Pts',(49.7371659252682,-0.742586235176362,
330.136393739505));
#63548=CARTESIAN_POINT('Ctrl Pts',(49.729754121091,-0.870598080429284,330.159417179218));
#63549=CARTESIAN_POINT('Ctrl Pts',(49.7219790423126,-1.00488416754517,330.183569066294));
#63550=CARTESIAN_POINT('Ctrl Pts',(49.7142039635341,-1.13837666874033,330.213351342367));
#63551=CARTESIAN_POINT('Ctrl Pts',(49.7064288847557,-1.27056654059029,330.248700837831));
#63552=CARTESIAN_POINT('Ctrl Pts',(49.6986633737067,-1.40259374438759,330.284006833489));
#63553=CARTESIAN_POINT('Ctrl Pts',(49.6908978626577,-1.53332113429082,330.324866317363));
#63554=CARTESIAN_POINT('Ctrl Pts',(49.6831323516087,-1.66224764308061,330.371164743094));
#63555=CARTESIAN_POINT('Ctrl Pts',(49.6753745400865,-1.79104632086087,330.417417263802));
#63556=CARTESIAN_POINT('Ctrl Pts',(49.6676167285643,-1.91804730542709,330.469097863282));
#63557=CARTESIAN_POINT('Ctrl Pts',(49.6598589170421,-2.04276288298187,330.526041700417));
#63558=CARTESIAN_POINT('Ctrl Pts',(49.6521069435191,-2.16738460810976,330.582942685508));
#63559=CARTESIAN_POINT('Ctrl Pts',(49.6443549699961,-2.28972399535329,330.645098862875));
#63560=CARTESIAN_POINT('Ctrl Pts',(49.6366029964731,-2.40931191483704,330.712296750063));
#63561=CARTESIAN_POINT('Ctrl Pts',(49.6288543059155,-2.52884918876582,330.779466178905));
#63562=CARTESIAN_POINT('Ctrl Pts',(49.6211056153578,-2.64563697247861,330.851672879791));
#63563=CARTESIAN_POINT('Ctrl Pts',(49.6133569248002,-2.75922962357171,330.928656862053));
#63564=CARTESIAN_POINT('Ctrl Pts',(49.6056098464224,-2.87279864076539,331.005624827156));
#63565=CARTESIAN_POINT('Ctrl Pts',(49.5978627680445,-2.98317352425808,331.087367877441));
#63566=CARTESIAN_POINT('Ctrl Pts',(49.5901156896667,-3.08993692356965,331.173582240416));
#63567=CARTESIAN_POINT('Ctrl Pts',(49.5823685463608,-3.1967012176614,331.25979732595));
#63568=CARTESIAN_POINT('Ctrl Pts',(49.574621403055,-3.29985366309907,331.350483553349));
#63569=CARTESIAN_POINT('Ctrl Pts',(49.5668742597492,-3.39900968034968,331.445296600926));
#63570=CARTESIAN_POINT('Ctrl Pts',(49.5591253747211,-3.49818798997778,331.540130964489));
#63571=CARTESIAN_POINT('Ctrl Pts',(49.551376489693,-3.59336780108802,331.639093724362));
#63572=CARTESIAN_POINT('Ctrl Pts',(49.5436276046649,-3.68420140608735,331.741803710351));
#63573=CARTESIAN_POINT('Ctrl Pts',(49.5358704948902,-3.77513142281352,331.84462271378));
#63574=CARTESIAN_POINT('Ctrl Pts',(49.5281133851154,-3.86170575896089,331.951196595182));
#63575=CARTESIAN_POINT('Ctrl Pts',(49.5203562753407,-3.943616694286,332.061110680708));
#63576=CARTESIAN_POINT('Ctrl Pts',(49.5125950204145,-4.0255714001959,332.171083500807));
#63577=CARTESIAN_POINT('Ctrl Pts',(49.5048337654884,-4.10285751967344,332.284399758847));
#63578=CARTESIAN_POINT('Ctrl Pts',(49.4970725105622,-4.17521128558254,332.400616653272));
#63579=CARTESIAN_POINT('Ctrl Pts',(49.4892988401575,-4.24768079393711,332.517019456854));
#63580=CARTESIAN_POINT('Ctrl Pts',(49.4815251697528,-4.31520198923567,332.636331828704));
#63581=CARTESIAN_POINT('Ctrl Pts',(49.4737514993482,-4.3775571844831,332.758086496075));
#63582=CARTESIAN_POINT('Ctrl Pts',(49.4663396951712,-4.43700973038937,332.874173454387));
#63583=CARTESIAN_POINT('Ctrl Pts',(49.4589278909942,-4.49176628638325,332.992480186322));
#63584=CARTESIAN_POINT('Ctrl Pts',(49.4515160868172,-4.54167993952892,333.112587382319));
#63585=CARTESIAN_POINT('Ctrl Pts',(49.442374527629,-4.60324236125915,333.260725003728));
#63586=CARTESIAN_POINT('Ctrl Pts',(49.4332329684409,-4.65761130890345,333.412019090102));
#63587=CARTESIAN_POINT('Ctrl Pts',(49.4240914092527,-4.70449014120338,333.565790958814));
#63588=CARTESIAN_POINT('Ctrl Pts',(49.4154417871895,-4.74884627059188,333.711287861579));
#63589=CARTESIAN_POINT('Ctrl Pts',(49.4067921651262,-4.7864970205464,333.859002619526));
#63590=CARTESIAN_POINT('Ctrl Pts',(49.3981425430629,-4.81723850715545,334.00833663591));
#63591=CARTESIAN_POINT('Ctrl Pts',(49.389518895868,-4.847887676891,334.157222201323));
#63592=CARTESIAN_POINT('Ctrl Pts',(49.3808952486729,-4.87166890175579,334.307717107534));
#63593=CARTESIAN_POINT('Ctrl Pts',(49.372271601478,-4.88842790078164,334.459208245847));
#63594=CARTESIAN_POINT('Ctrl Pts',(49.3636874533892,-4.90511013814649,334.610005505524));
#63595=CARTESIAN_POINT('Ctrl Pts',(49.3551033053004,-4.91483423476958,334.761789673102));
#63596=CARTESIAN_POINT('Ctrl Pts',(49.3465191572117,-4.91749699019781,334.913939475394));
#63597=CARTESIAN_POINT('Ctrl Pts',(49.3449518969943,-4.91798314567977,334.941718391805));
#63598=CARTESIAN_POINT('Ctrl Pts',(49.3433846367768,-4.91823405249636,334.969509456849));
#63599=CARTESIAN_POINT('Ctrl Pts',(49.3418173765594,-4.91824926372691,334.997308838587));
#63600=CARTESIAN_POINT('',(47.5918173764616,-4.91824832477837,335.004059349057));
#63601=CARTESIAN_POINT('Ctrl Pts',(49.3418173765087,-4.9182492637274,334.997308839488));
#63602=CARTESIAN_POINT('Ctrl Pts',(49.3339770743027,-4.918325358688,335.136376718293));
#63603=CARTESIAN_POINT('Ctrl Pts',(49.3261367720966,-4.91249870650781,335.275447231013));
#63604=CARTESIAN_POINT('Ctrl Pts',(49.3182964698906,-4.90079520016747,335.413992111659));
#63605=CARTESIAN_POINT('Ctrl Pts',(49.3104544424886,-4.88908911856388,335.552567478));
#63606=CARTESIAN_POINT('Ctrl Pts',(49.3026124150866,-4.87150363858987,335.690616605482));
#63607=CARTESIAN_POINT('Ctrl Pts',(49.2947703876846,-4.84811653661624,335.82761652345));
#63608=CARTESIAN_POINT('Ctrl Pts',(49.2869250969572,-4.82471970250068,335.964673451588));
#63609=CARTESIAN_POINT('Ctrl Pts',(49.2790798062298,-4.79551650137673,336.100679928484));
#63610=CARTESIAN_POINT('Ctrl Pts',(49.2712345155024,-4.7606357602937,336.235123564795));
#63611=CARTESIAN_POINT('Ctrl Pts',(49.2630714769224,-4.72434228882767,336.375012401063));
#63612=CARTESIAN_POINT('Ctrl Pts',(49.2549084383425,-4.68190184646951,336.513208706157));
#63613=CARTESIAN_POINT('Ctrl Pts',(49.2467453997626,-4.63351621607897,336.649154491803));
#63614=CARTESIAN_POINT('Ctrl Pts',(49.2388840795037,-4.58691899217707,336.780075514452));
#63615=CARTESIAN_POINT('Ctrl Pts',(49.2310227592448,-4.53480843673019,336.908909094979));
#63616=CARTESIAN_POINT('Ctrl Pts',(49.2231614389859,-4.47741306156182,337.035179436476));
#63617=CARTESIAN_POINT('Ctrl Pts',(49.2152934719634,-4.41996915847789,337.161556539824));
#63618=CARTESIAN_POINT('Ctrl Pts',(49.2074255049411,-4.35723170070286,337.285365749583));
#63619=CARTESIAN_POINT('Ctrl Pts',(49.1995575379187,-4.28947437167885,337.406157242827));
#63620=CARTESIAN_POINT('Ctrl Pts',(49.1916774945105,-4.22161304328106,337.527134136527));
#63621=CARTESIAN_POINT('Ctrl Pts',(49.1837974511023,-4.14871665890939,337.645083747083));
#63622=CARTESIAN_POINT('Ctrl Pts',(49.1759174076941,-4.07110155546219,337.759586053671));
#63623=CARTESIAN_POINT('Ctrl Pts',(49.1750376226438,-4.0624360438459,337.772369919487));
#63624=CARTESIAN_POINT('Ctrl Pts',(49.1741578375935,-4.05371175306366,337.785110849596));
#63625=CARTESIAN_POINT('Ctrl Pts',(49.1732780525432,-4.04492915320926,337.797808286502));
#63626=CARTESIAN_POINT('Ctrl Pts',(49.1655029737647,-3.96731314265758,337.910021573363));
#63627=CARTESIAN_POINT('Ctrl Pts',(49.1577278949863,-3.8849014615822,338.019179929276));
#63628=CARTESIAN_POINT('Ctrl Pts',(49.1499528162079,-3.7979624986255,338.124846223662));
#63629=CARTESIAN_POINT('Ctrl Pts',(49.1421873051589,-3.71113051959753,338.230382488945));
#63630=CARTESIAN_POINT('Ctrl Pts',(49.1344217941098,-3.61978258956768,338.33243494395));
#63631=CARTESIAN_POINT('Ctrl Pts',(49.1266562830608,-3.52423055277304,338.430595002824));
#63632=CARTESIAN_POINT('Ctrl Pts',(49.1188984715386,-3.42877325610114,338.528657735714));
#63633=CARTESIAN_POINT('Ctrl Pts',(49.1111406600165,-3.32912041887219,338.622835474462));
#63634=CARTESIAN_POINT('Ctrl Pts',(49.1033828484943,-3.22562412838877,338.712752623709));
#63635=CARTESIAN_POINT('Ctrl Pts',(49.0956308749713,-3.12220572214578,338.802602107449));
#63636=CARTESIAN_POINT('Ctrl Pts',(49.0878789014482,-3.01494991355094,338.888197128208));
#63637=CARTESIAN_POINT('Ctrl Pts',(49.0801269279252,-2.90424536113982,338.969199156605));
#63638=CARTESIAN_POINT('Ctrl Pts',(49.0723782373676,-2.79358769217252,339.050166880595));
#63639=CARTESIAN_POINT('Ctrl Pts',(49.0646295468099,-2.67948449910283,339.126545250627));
#63640=CARTESIAN_POINT('Ctrl Pts',(49.0568808562523,-2.56235703872575,339.198036382476));
#63641=CARTESIAN_POINT('Ctrl Pts',(49.0491337778745,-2.44525394769507,339.269512639998));
#63642=CARTESIAN_POINT('Ctrl Pts',(49.0413866994967,-2.32512817435458,339.336103478371));
#63643=CARTESIAN_POINT('Ctrl Pts',(49.0336396211189,-2.20242910188921,339.397554901721));
#63644=CARTESIAN_POINT('Ctrl Pts',(49.0258924778131,-2.07972900108753,339.459006840094));
#63645=CARTESIAN_POINT('Ctrl Pts',(49.0181453345072,-1.95445590763695,339.515319102494));
#63646=CARTESIAN_POINT('Ctrl Pts',(49.0103981912014,-1.82708253330984,339.566284318675));
#63647=CARTESIAN_POINT('Ctrl Pts',(49.0026493061733,-1.69968052274406,339.617260992918));
#63648=CARTESIAN_POINT('Ctrl Pts',(48.9949004211453,-1.57017765453207,339.662888083659));
#63649=CARTESIAN_POINT('Ctrl Pts',(48.9871515361172,-1.43906490185854,339.703007045576));
#63650=CARTESIAN_POINT('Ctrl Pts',(48.9793944263425,-1.30781298475477,339.743168590174));
#63651=CARTESIAN_POINT('Ctrl Pts',(48.9716373165678,-1.17494814416339,339.777810212697));
#63652=CARTESIAN_POINT('Ctrl Pts',(48.963880206793,-1.04097527968342,339.806823642447));
#63653=CARTESIAN_POINT('Ctrl Pts',(48.9561189518669,-0.906930824388212,
339.835852576047));
#63654=CARTESIAN_POINT('Ctrl Pts',(48.9483576969407,-0.771777550358167,
339.859247257473));
#63655=CARTESIAN_POINT('Ctrl Pts',(48.9405964420145,-0.636027747730289,
339.876951072814));
#63656=CARTESIAN_POINT('Ctrl Pts',(48.9328227716099,-0.500060789658963,
339.894683208489));
#63657=CARTESIAN_POINT('Ctrl Pts',(48.9250491012052,-0.363495785686038,
339.906706252232));
#63658=CARTESIAN_POINT('Ctrl Pts',(48.9172754308006,-0.226848207315626,
339.913015667931));
#63659=CARTESIAN_POINT('Ctrl Pts',(48.9098636266235,-0.0965616065939597,
339.919031378812));
#63660=CARTESIAN_POINT('Ctrl Pts',(48.9024518224464,0.0337997660645954,
339.919853427656));
#63661=CARTESIAN_POINT('Ctrl Pts',(48.8950400182694,0.163793413952805,339.915521821744));
#63662=CARTESIAN_POINT('Ctrl Pts',(48.8872649394909,0.300158437755397,339.910977910924));
#63663=CARTESIAN_POINT('Ctrl Pts',(48.8794898607125,0.436549717445622,339.900748020022));
#63664=CARTESIAN_POINT('Ctrl Pts',(48.871714781934,0.572454420098576,339.884821286333));
#63665=CARTESIAN_POINT('Ctrl Pts',(48.863949270885,0.708191883362706,339.868914151503));
#63666=CARTESIAN_POINT('Ctrl Pts',(48.856183759836,0.843443576451924,339.84732416749));
#63667=CARTESIAN_POINT('Ctrl Pts',(48.848418248787,0.977697153996748,339.820092461516));
#63668=CARTESIAN_POINT('Ctrl Pts',(48.8406604372648,1.11181761872857,339.792887755858));
#63669=CARTESIAN_POINT('Ctrl Pts',(48.8329026257426,1.24494155673891,339.760052537386));
#63670=CARTESIAN_POINT('Ctrl Pts',(48.8251448142204,1.37656258723531,339.721679627624));
#63671=CARTESIAN_POINT('Ctrl Pts',(48.8173928406974,1.50808456873214,339.683335594694));
#63672=CARTESIAN_POINT('Ctrl Pts',(48.8096408671744,1.63810552014544,339.639462274219));
#63673=CARTESIAN_POINT('Ctrl Pts',(48.8018888936514,1.76613043946227,339.590203299779));
#63674=CARTESIAN_POINT('Ctrl Pts',(48.7941402030938,1.89410114014984,339.540965186545));
#63675=CARTESIAN_POINT('Ctrl Pts',(48.7863915125361,2.02007712598061,339.486346095822));
#63676=CARTESIAN_POINT('Ctrl Pts',(48.7786428219785,2.14357993353085,339.42653906919));
#63677=CARTESIAN_POINT('Ctrl Pts',(48.7708957436007,2.26705704529046,339.366744485909));
#63678=CARTESIAN_POINT('Ctrl Pts',(48.7631486652229,2.38806165070146,339.301764283961));
#63679=CARTESIAN_POINT('Ctrl Pts',(48.755401586845,2.50613697218775,339.231838907512));
#63680=CARTESIAN_POINT('Ctrl Pts',(48.7476544435392,2.62421328325871,339.161912945021));
#63681=CARTESIAN_POINT('Ctrl Pts',(48.7399073002334,2.73935992511543,339.087041924536));
#63682=CARTESIAN_POINT('Ctrl Pts',(48.7321601569276,2.85114670422752,339.007511139532));
#63683=CARTESIAN_POINT('Ctrl Pts',(48.7244112718995,2.96295861538101,338.927962474318));
#63684=CARTESIAN_POINT('Ctrl Pts',(48.7166623868714,3.07140884225921,338.843752186498));
#63685=CARTESIAN_POINT('Ctrl Pts',(48.7089135018433,3.17609836695589,338.755207347926));
#63686=CARTESIAN_POINT('Ctrl Pts',(48.7011563920686,3.28089901019566,338.666568526948));
#63687=CARTESIAN_POINT('Ctrl Pts',(48.6933992822939,3.38193067864855,338.573586217631));
#63688=CARTESIAN_POINT('Ctrl Pts',(48.6856421725192,3.47882909503142,338.476626409332));
#63689=CARTESIAN_POINT('Ctrl Pts',(48.677880917593,3.57577929083006,338.379614788811));
#63690=CARTESIAN_POINT('Ctrl Pts',(48.6701196626668,3.66859156921593,338.278621721817));
#63691=CARTESIAN_POINT('Ctrl Pts',(48.6623584077407,3.75694109275471,338.174047367018));
#63692=CARTESIAN_POINT('Ctrl Pts',(48.654584737336,3.84543194673788,338.069305727332));
#63693=CARTESIAN_POINT('Ctrl Pts',(48.6468110669313,3.92944554046913,337.960971660855));
#63694=CARTESIAN_POINT('Ctrl Pts',(48.6390373965267,4.00869910822896,337.849476183825));
#63695=CARTESIAN_POINT('Ctrl Pts',(48.6316255923496,4.08426340334254,337.743170848074));
#63696=CARTESIAN_POINT('Ctrl Pts',(48.6242137881725,4.15550070063262,337.633992046465));
#63697=CARTESIAN_POINT('Ctrl Pts',(48.6168019839954,4.22220518271761,337.522333534157));
#63698=CARTESIAN_POINT('Ctrl Pts',(48.6090269052169,4.29217905017198,337.405202305547));
#63699=CARTESIAN_POINT('Ctrl Pts',(48.6012518264385,4.35738566423734,337.284971987716));
#63700=CARTESIAN_POINT('Ctrl Pts',(48.59347674766,4.41753836691207,337.162067954381));
#63701=CARTESIAN_POINT('Ctrl Pts',(48.585711236611,4.47761704785652,337.039315162283));
#63702=CARTESIAN_POINT('Ctrl Pts',(48.577945725562,4.53265402156882,336.913895548913));
#63703=CARTESIAN_POINT('Ctrl Pts',(48.570180214513,4.58240661333048,336.786262212724));
#63704=CARTESIAN_POINT('Ctrl Pts',(48.5624224029907,4.63210987525269,336.658755425359));
#63705=CARTESIAN_POINT('Ctrl Pts',(48.5546645914685,4.67653904103847,336.529039645011));
#63706=CARTESIAN_POINT('Ctrl Pts',(48.5469067799463,4.7154981345845,336.397590929146));
#63707=CARTESIAN_POINT('Ctrl Pts',(48.5391548064233,4.75442791017694,336.266241132608));
#63708=CARTESIAN_POINT('Ctrl Pts',(48.5314028329004,4.78789569640302,336.13316136953));
#63709=CARTESIAN_POINT('Ctrl Pts',(48.5236508593774,4.81575440381345,335.998845626036));
#63710=CARTESIAN_POINT('Ctrl Pts',(48.5159021688198,4.84360131304485,335.864586765339));
#63711=CARTESIAN_POINT('Ctrl Pts',(48.5081534782621,4.86584378884237,335.729093347241));
#63712=CARTESIAN_POINT('Ctrl Pts',(48.5004047877045,4.88238523997546,335.592872187718));
#63713=CARTESIAN_POINT('Ctrl Pts',(48.4926577093267,4.89892324952146,335.456679370145));
#63714=CARTESIAN_POINT('Ctrl Pts',(48.4849106309489,4.90976254664243,335.319759500098));
#63715=CARTESIAN_POINT('Ctrl Pts',(48.4771635525711,4.91485813741064,335.18262680972));
#63716=CARTESIAN_POINT('Ctrl Pts',(48.4694164092653,4.9199537708848,335.045492970038));
#63717=CARTESIAN_POINT('Ctrl Pts',(48.4616692659594,4.91930558747766,334.908146697072));
#63718=CARTESIAN_POINT('Ctrl Pts',(48.4539221226536,4.91292069415397,334.771104138409));
#63719=CARTESIAN_POINT('Ctrl Pts',(48.4461732376256,4.90653436537073,334.634030769669));
#63720=CARTESIAN_POINT('Ctrl Pts',(48.4384243525975,4.89440877843182,334.497261641479));
#63721=CARTESIAN_POINT('Ctrl Pts',(48.4306754675695,4.87660304355248,334.361309293856));
#63722=CARTESIAN_POINT('Ctrl Pts',(48.4229183577947,4.85877840948209,334.225212645006));
#63723=CARTESIAN_POINT('Ctrl Pts',(48.41516124802,4.83526163488226,334.089934896692));
#63724=CARTESIAN_POINT('Ctrl Pts',(48.4074041382453,4.80616335667175,333.955980435296));
#63725=CARTESIAN_POINT('Ctrl Pts',(48.3996428833192,4.77704952927181,333.821954392918));
#63726=CARTESIAN_POINT('Ctrl Pts',(48.391881628393,4.74234835404569,333.689253424429));
#63727=CARTESIAN_POINT('Ctrl Pts',(48.3841203734669,4.70222054478059,333.558367241374));
#63728=CARTESIAN_POINT('Ctrl Pts',(48.3763467030622,4.66202854409822,333.427271683082));
#63729=CARTESIAN_POINT('Ctrl Pts',(48.3685730326576,4.61639269265932,333.297997080184));
#63730=CARTESIAN_POINT('Ctrl Pts',(48.3607993622529,4.56552242045621,333.171014464023));
#63731=CARTESIAN_POINT('Ctrl Pts',(48.3533875580758,4.51702017166269,333.049942919195));
#63732=CARTESIAN_POINT('Ctrl Pts',(48.3459757538987,4.46375997732151,332.930955041894));
#63733=CARTESIAN_POINT('Ctrl Pts',(48.3385639497216,4.40596157494998,332.814436991857));
#63734=CARTESIAN_POINT('Ctrl Pts',(48.3307888709431,4.34533030070588,332.692208045098));
#63735=CARTESIAN_POINT('Ctrl Pts',(48.3230137921647,4.27951310186669,332.572310888417));
#63736=CARTESIAN_POINT('Ctrl Pts',(48.3152387133863,4.20871255717112,332.455216772766));
#63737=CARTESIAN_POINT('Ctrl Pts',(48.3074732023373,4.13799913705294,332.338266748879));
#63738=CARTESIAN_POINT('Ctrl Pts',(48.2997076912882,4.06231477295682,332.224113234152));
#63739=CARTESIAN_POINT('Ctrl Pts',(48.2919421802392,3.98190915982253,332.113205496503));
#63740=CARTESIAN_POINT('Ctrl Pts',(48.284184368717,3.90158326908809,332.002407724199));
#63741=CARTESIAN_POINT('Ctrl Pts',(48.2764265571948,3.81654567298116,331.894849639));
#63742=CARTESIAN_POINT('Ctrl Pts',(48.2686687456726,3.72709064446503,331.790953663401));
#63743=CARTESIAN_POINT('Ctrl Pts',(48.2609167721496,3.63770293369469,331.687135872818));
#63744=CARTESIAN_POINT('Ctrl Pts',(48.2531647986267,3.54390466129782,331.58697500146));
#63745=CARTESIAN_POINT('Ctrl Pts',(48.2454128251037,3.44603163220536,331.490862064219));
#63746=CARTESIAN_POINT('Ctrl Pts',(48.2376641345461,3.3482000523987,331.394789830863));
#63747=CARTESIAN_POINT('Ctrl Pts',(48.2299154439884,3.24629742642207,331.302762395299));
#63748=CARTESIAN_POINT('Ctrl Pts',(48.2221667534308,3.14069767558466,331.215135250359));
#63749=CARTESIAN_POINT('Ctrl Pts',(48.214419675053,3.0351198956574,331.127526336978));
#63750=CARTESIAN_POINT('Ctrl Pts',(48.2066725966751,2.92584682150826,331.044316142639));
#63751=CARTESIAN_POINT('Ctrl Pts',(48.1989255182973,2.81328653312129,330.965820784217));
#63752=CARTESIAN_POINT('Ctrl Pts',(48.1911783749915,2.70072530137045,330.887324767927));
#63753=CARTESIAN_POINT('Ctrl Pts',(48.1834312316857,2.58487712104461,330.813543889953));
#63754=CARTESIAN_POINT('Ctrl Pts',(48.1756840883799,2.46617987764701,330.744751490972));
#63755=CARTESIAN_POINT('Ctrl Pts',(48.1679352033518,2.3474559485894,330.675943625998));
#63756=CARTESIAN_POINT('Ctrl Pts',(48.1601863183237,2.22588201999382,330.612126667668));
#63757=CARTESIAN_POINT('Ctrl Pts',(48.1524374332956,2.10192108562494,330.553528273754));
#63758=CARTESIAN_POINT('Ctrl Pts',(48.1446803235208,1.97782857783931,330.494867682899));
#63759=CARTESIAN_POINT('Ctrl Pts',(48.1369232137461,1.85134435712972,330.44143688852));
#63760=CARTESIAN_POINT('Ctrl Pts',(48.1291661039714,1.72295244474943,330.393415806085));
#63761=CARTESIAN_POINT('Ctrl Pts',(48.1214048490452,1.59449192383661,330.345369062718));
#63762=CARTESIAN_POINT('Ctrl Pts',(48.113643594119,1.4641220513151,330.302737912853));
#63763=CARTESIAN_POINT('Ctrl Pts',(48.1058823391928,1.3323416075233,330.265652219855));
#63764=CARTESIAN_POINT('Ctrl Pts',(48.0981086687882,1.2003503579684,330.228507201834));
#63765=CARTESIAN_POINT('Ctrl Pts',(48.0903349983835,1.06694440864054,330.196925457504));
#63766=CARTESIAN_POINT('Ctrl Pts',(48.0825613279789,0.932633194431056,330.170985774804));
#63767=CARTESIAN_POINT('Ctrl Pts',(48.0751495238017,0.804574199555421,330.146253590574));
#63768=CARTESIAN_POINT('Ctrl Pts',(48.0677377196246,0.675692607809895,330.126650056321));
#63769=CARTESIAN_POINT('Ctrl Pts',(48.0603259154474,0.546432061734352,330.112199363271));
#63770=CARTESIAN_POINT('Ctrl Pts',(48.052550836669,0.410836071249504,330.097040398708));
#63771=CARTESIAN_POINT('Ctrl Pts',(48.0447757578906,0.274394531420278,330.087504254182));
#63772=CARTESIAN_POINT('Ctrl Pts',(48.0370006791121,0.137613354207217,330.083675597843));
#63773=CARTESIAN_POINT('Ctrl Pts',(48.0292351680631,0.00100049494072593,
330.079851652909));
#63774=CARTESIAN_POINT('Ctrl Pts',(48.0214696570141,-0.135950783131938,
330.081721232386));
#63775=CARTESIAN_POINT('Ctrl Pts',(48.0137041459651,-0.272727556773448,
330.089317487123));
#63776=CARTESIAN_POINT('Ctrl Pts',(48.0059463344429,-0.40936871584577,330.096906210151));
#63777=CARTESIAN_POINT('Ctrl Pts',(47.9981885229207,-0.545835327050987,
330.110210287332));
#63778=CARTESIAN_POINT('Ctrl Pts',(47.9904307113985,-0.681612918314197,
330.129210855304));
#63779=CARTESIAN_POINT('Ctrl Pts',(47.9826787378755,-0.817288332634226,
330.148197124747));
#63780=CARTESIAN_POINT('Ctrl Pts',(47.9749267643525,-0.952275373536065,
330.172871298382));
#63781=CARTESIAN_POINT('Ctrl Pts',(47.9671747908295,-1.08606350493718,330.203162591275));
#63782=CARTESIAN_POINT('Ctrl Pts',(47.9594261002719,-1.2197949769853,330.233441055788));
#63783=CARTESIAN_POINT('Ctrl Pts',(47.9516774097142,-1.35232816895784,330.269331822052));
#63784=CARTESIAN_POINT('Ctrl Pts',(47.9439287191566,-1.48316178907224,330.310712829231));
#63785=CARTESIAN_POINT('Ctrl Pts',(47.9361816407788,-1.61396818815906,330.352085226746));
#63786=CARTESIAN_POINT('Ctrl Pts',(47.928434562401,-1.74307534629962,330.398945475281));
#63787=CARTESIAN_POINT('Ctrl Pts',(47.9206874840232,-1.86999659857624,330.451121480649));
#63788=CARTESIAN_POINT('Ctrl Pts',(47.9129403407174,-1.99691891457528,330.503297923302));
#63789=CARTESIAN_POINT('Ctrl Pts',(47.9051931974116,-2.121654926651,330.560790063033));
#63790=CARTESIAN_POINT('Ctrl Pts',(47.8974460541058,-2.24373781182481,330.623377592905));
#63791=CARTESIAN_POINT('Ctrl Pts',(47.8896971690777,-2.36584814382302,330.685979193782));
#63792=CARTESIAN_POINT('Ctrl Pts',(47.8819482840495,-2.48530381423137,330.753678286036));
#63793=CARTESIAN_POINT('Ctrl Pts',(47.8741993990214,-2.60166282827983,330.826208727015));
#63794=CARTESIAN_POINT('Ctrl Pts',(47.8664422892467,-2.71814534698785,330.898816152553));
#63795=CARTESIAN_POINT('Ctrl Pts',(47.858685179472,-2.83152431136569,330.976264963474));
#63796=CARTESIAN_POINT('Ctrl Pts',(47.8509280696973,-2.94138649498551,331.058245498561));
#63797=CARTESIAN_POINT('Ctrl Pts',(47.8431668147711,-3.05130738544384,331.140269841425));
#63798=CARTESIAN_POINT('Ctrl Pts',(47.835405559845,-3.15770744750401,331.226830487181));
#63799=CARTESIAN_POINT('Ctrl Pts',(47.8276443049188,-3.26020755763102,331.31757827732));
#63800=CARTESIAN_POINT('Ctrl Pts',(47.8198706345141,-3.36287163452938,331.408471234349));
#63801=CARTESIAN_POINT('Ctrl Pts',(47.8120969641094,-3.46162301111644,331.503564449213));
#63802=CARTESIAN_POINT('Ctrl Pts',(47.8043232937048,-3.55611974848233,331.602472163918));
#63803=CARTESIAN_POINT('Ctrl Pts',(47.7969114895277,-3.64621763998886,331.696775700707));
#63804=CARTESIAN_POINT('Ctrl Pts',(47.7894996853507,-3.73244789468158,331.794546383538));
#63805=CARTESIAN_POINT('Ctrl Pts',(47.7820878811736,-3.81455008920872,331.895424235194));
#63806=CARTESIAN_POINT('Ctrl Pts',(47.7741599434793,-3.90236960888749,332.003326886636));
#63807=CARTESIAN_POINT('Ctrl Pts',(47.7662320057849,-3.98575743039446,332.115143472683));
#63808=CARTESIAN_POINT('Ctrl Pts',(47.7583040680905,-4.06434425910569,332.230471374769));
#63809=CARTESIAN_POINT('Ctrl Pts',(47.7505666293383,-4.1410427395082,332.343028084119));
#63810=CARTESIAN_POINT('Ctrl Pts',(47.7428291905861,-4.21316804587119,332.458928960272));
#63811=CARTESIAN_POINT('Ctrl Pts',(47.7350917518339,-4.28041534114292,332.577763931858));
#63812=CARTESIAN_POINT('Ctrl Pts',(47.7273617014445,-4.3475984229928,332.696485429732));
#63813=CARTESIAN_POINT('Ctrl Pts',(47.7196316510551,-4.40991256644573,332.818135110118));
#63814=CARTESIAN_POINT('Ctrl Pts',(47.7119016006658,-4.46709565679131,332.942273231069));
#63815=CARTESIAN_POINT('Ctrl Pts',(47.7041772301748,-4.52423673005729,333.066320137619));
#63816=CARTESIAN_POINT('Ctrl Pts',(47.6964528596838,-4.57625408746932,333.192851490939));
#63817=CARTESIAN_POINT('Ctrl Pts',(47.6887284891928,-4.62293129577608,333.321402580416));
#63818=CARTESIAN_POINT('Ctrl Pts',(47.6806525631358,-4.67173290145687,333.455804353917));
#63819=CARTESIAN_POINT('Ctrl Pts',(47.6725766370788,-4.7146966125614,333.59241364941));
#63820=CARTESIAN_POINT('Ctrl Pts',(47.6645007110218,-4.75163105817567,333.730675238767));
#63821=CARTESIAN_POINT('Ctrl Pts',(47.6567817387722,-4.786933011009,333.862825702241));
#63822=CARTESIAN_POINT('Ctrl Pts',(47.6490627665226,-4.81672717171253,333.996485105244));
#63823=CARTESIAN_POINT('Ctrl Pts',(47.641343794273,-4.84089748737306,334.131153305096));
#63824=CARTESIAN_POINT('Ctrl Pts',(47.6336254228008,-4.86506592182759,334.265811023553));
#63825=CARTESIAN_POINT('Ctrl Pts',(47.6259070513286,-4.88361131809932,334.401476994412));
#63826=CARTESIAN_POINT('Ctrl Pts',(47.6181886798563,-4.89646894791932,334.537642016872));
#63827=CARTESIAN_POINT('Ctrl Pts',(47.6104678657073,-4.90933064686615,334.673850132248));
#63828=CARTESIAN_POINT('Ctrl Pts',(47.6027470515583,-4.9165009547583,334.810557222311));
#63829=CARTESIAN_POINT('Ctrl Pts',(47.5950262374094,-4.91796711350799,334.947250280058));
#63830=CARTESIAN_POINT('Ctrl Pts',(47.5939566171091,-4.91817023109789,334.966187359315));
#63831=CARTESIAN_POINT('Ctrl Pts',(47.5928869968089,-4.91826395320588,334.985124169515));
#63832=CARTESIAN_POINT('Ctrl Pts',(47.5918173765087,-4.91824832477906,335.004059348224));
#63833=CARTESIAN_POINT('',(45.8418173765417,-4.91824993362185,335.000808040044));
#63834=CARTESIAN_POINT('Ctrl Pts',(47.5918173764616,-4.91824832477837,335.004059349057));
#63835=CARTESIAN_POINT('Ctrl Pts',(47.5826404069209,-4.91811423829332,335.166516585725));
#63836=CARTESIAN_POINT('Ctrl Pts',(47.5734634373801,-4.90992702535072,335.328629453609));
#63837=CARTESIAN_POINT('Ctrl Pts',(47.5642864678394,-4.89381185941993,335.489682087788));
#63838=CARTESIAN_POINT('Ctrl Pts',(47.5550435007526,-4.87758079886826,335.651892956022));
#63839=CARTESIAN_POINT('Ctrl Pts',(47.5458005336658,-4.8533074482954,335.813028237604));
#63840=CARTESIAN_POINT('Ctrl Pts',(47.536557566579,-4.82116847162421,335.972377308824));
#63841=CARTESIAN_POINT('Ctrl Pts',(47.5272433712864,-4.78878182538708,336.13295435677));
#63842=CARTESIAN_POINT('Ctrl Pts',(47.5179291759937,-4.74840792014492,336.291717514412));
#63843=CARTESIAN_POINT('Ctrl Pts',(47.508614980701,-4.70027563195492,336.447961341387));
#63844=CARTESIAN_POINT('Ctrl Pts',(47.5070266027672,-4.69206748706824,336.474606074428));
#63845=CARTESIAN_POINT('Ctrl Pts',(47.5054382248335,-4.68363382787156,336.501177593195));
#63846=CARTESIAN_POINT('Ctrl Pts',(47.5038498468996,-4.67497592595325,336.527672463016));
#63847=CARTESIAN_POINT('Ctrl Pts',(47.4960747681212,-4.6325956661689,336.657364330235));
#63848=CARTESIAN_POINT('Ctrl Pts',(47.4882996893428,-4.5847475352392,336.785496247453));
#63849=CARTESIAN_POINT('Ctrl Pts',(47.4805246105644,-4.53156407116226,336.91157268537));
#63850=CARTESIAN_POINT('Ctrl Pts',(47.4727590995154,-4.47844605272372,337.037493978203));
#63851=CARTESIAN_POINT('Ctrl Pts',(47.4649935884664,-4.42000591500347,337.161364467814));
#63852=CARTESIAN_POINT('Ctrl Pts',(47.4572280774174,-4.35642598878991,337.28270358713));
#63853=CARTESIAN_POINT('Ctrl Pts',(47.4494702658952,-4.29290910225829,337.403922398356));
#63854=CARTESIAN_POINT('Ctrl Pts',(47.4417124543731,-4.2242627490384,337.52261449006));
#63855=CARTESIAN_POINT('Ctrl Pts',(47.4339546428509,-4.15071724189254,337.638319434859));
#63856=CARTESIAN_POINT('Ctrl Pts',(47.4262026693279,-4.07722708007316,337.753937308018));
#63857=CARTESIAN_POINT('Ctrl Pts',(47.4184506958049,-3.99884531149489,337.866572180107));
#63858=CARTESIAN_POINT('Ctrl Pts',(47.4106987222819,-3.91584787423138,337.975788717026));
#63859=CARTESIAN_POINT('Ctrl Pts',(47.4029500317243,-3.83288558643161,338.084959000676));
#63860=CARTESIAN_POINT('Ctrl Pts',(47.3952013411667,-3.74531175379001,338.190713517903));
#63861=CARTESIAN_POINT('Ctrl Pts',(47.387452650609,-3.65344515282044,338.2926465917));
#63862=CARTESIAN_POINT('Ctrl Pts',(47.3797055722312,-3.56159766546455,338.394558457469));
#63863=CARTESIAN_POINT('Ctrl Pts',(47.3719584938535,-3.46545944782824,338.492650171113));
#63864=CARTESIAN_POINT('Ctrl Pts',(47.3642114154757,-3.36538875398464,338.586550096828));
#63865=CARTESIAN_POINT('Ctrl Pts',(47.3564642721699,-3.26531722145224,338.680450809514));
#63866=CARTESIAN_POINT('Ctrl Pts',(47.3487171288641,-3.1613134320139,338.770159396739));
#63867=CARTESIAN_POINT('Ctrl Pts',(47.3409699855583,-3.05377129970843,338.855342256088));
#63868=CARTESIAN_POINT('Ctrl Pts',(47.3332211005302,-2.94620498964865,338.940544266352));
#63869=CARTESIAN_POINT('Ctrl Pts',(47.3254722155021,-2.83509906011699,339.021218281422));
#63870=CARTESIAN_POINT('Ctrl Pts',(47.317723330474,-2.72087885587924,339.097072285685));
#63871=CARTESIAN_POINT('Ctrl Pts',(47.3099662206993,-2.60653741713644,339.173006802172));
#63872=CARTESIAN_POINT('Ctrl Pts',(47.3022091109246,-2.48907542672063,339.244110871563));
#63873=CARTESIAN_POINT('Ctrl Pts',(47.2944520011499,-2.36894591880351,339.310136691137));
#63874=CARTESIAN_POINT('Ctrl Pts',(47.2866907462237,-2.24875221751827,339.376197792798));
#63875=CARTESIAN_POINT('Ctrl Pts',(47.2789294912976,-2.12588850836958,339.437175063762));
#63876=CARTESIAN_POINT('Ctrl Pts',(47.2711682363714,-2.00082964491927,339.492868103396));
#63877=CARTESIAN_POINT('Ctrl Pts',(47.2633945659668,-1.87557072804404,339.548650233743));
#63878=CARTESIAN_POINT('Ctrl Pts',(47.2556208955621,-1.74811000338902,339.599131097061));
#63879=CARTESIAN_POINT('Ctrl Pts',(47.2478472251574,-1.61894022973554,339.64415929906));
#63880=CARTESIAN_POINT('Ctrl Pts',(47.2404354209802,-1.4957833401193,339.687091427424));
#63881=CARTESIAN_POINT('Ctrl Pts',(47.2330236168029,-1.37107320855419,339.725067029216));
#63882=CARTESIAN_POINT('Ctrl Pts',(47.2256118126257,-1.2452453579823,339.757998219937));
#63883=CARTESIAN_POINT('Ctrl Pts',(47.2178367338473,-1.11325030963496,339.792543466411));
#63884=CARTESIAN_POINT('Ctrl Pts',(47.2100616550688,-0.97960807770071,339.821646484932));
#63885=CARTESIAN_POINT('Ctrl Pts',(47.2022865762904,-0.844807087254626,
339.845150570191));
#63886=CARTESIAN_POINT('Ctrl Pts',(47.1945210652414,-0.710171978009045,
339.868625732178));
#63887=CARTESIAN_POINT('Ctrl Pts',(47.1867555541924,-0.574381328819445,
339.886515603218));
#63888=CARTESIAN_POINT('Ctrl Pts',(47.1789900431434,-0.437937928439986,
339.898713446746));
#63889=CARTESIAN_POINT('Ctrl Pts',(47.1712322316212,-0.301629812089341,
339.910899196077));
#63890=CARTESIAN_POINT('Ctrl Pts',(47.163474420099,-0.164670619336524,339.91740411452));
#63891=CARTESIAN_POINT('Ctrl Pts',(47.1557166085768,-0.0275721688405922,
339.918172713316));
#63892=CARTESIAN_POINT('Ctrl Pts',(47.1479646350538,0.1094231107237,339.918940733717));
#63893=CARTESIAN_POINT('Ctrl Pts',(47.1402126615308,0.246557050145736,339.913981024592));
#63894=CARTESIAN_POINT('Ctrl Pts',(47.1324606880078,0.383314241768882,339.903290043895));
#63895=CARTESIAN_POINT('Ctrl Pts',(47.1247119974501,0.520013516640182,339.892603590834));
#63896=CARTESIAN_POINT('Ctrl Pts',(47.1169633068925,0.656335972177747,339.876190724124));
#63897=CARTESIAN_POINT('Ctrl Pts',(47.1092146163349,0.79176795766934,339.854099974631));
#63898=CARTESIAN_POINT('Ctrl Pts',(47.1014675379571,0.927171765405202,339.832013821302));
#63899=CARTESIAN_POINT('Ctrl Pts',(47.0937204595792,1.06168508607588,339.804252197826));
#63900=CARTESIAN_POINT('Ctrl Pts',(47.0859733812014,1.19480153137067,339.770915254239));
#63901=CARTESIAN_POINT('Ctrl Pts',(47.0782262378956,1.32791909230939,339.737578031257));
#63902=CARTESIAN_POINT('Ctrl Pts',(47.0704790945898,1.45963937535645,339.698665489919));
#63903=CARTESIAN_POINT('Ctrl Pts',(47.062731951284,1.58946867763668,339.654328349538));
#63904=CARTESIAN_POINT('Ctrl Pts',(47.0549830662559,1.71932716830042,339.609981241226));
#63905=CARTESIAN_POINT('Ctrl Pts',(47.0472341812278,1.84729346240389,339.56020723337));
#63906=CARTESIAN_POINT('Ctrl Pts',(47.0394852961997,1.97289181933021,339.505205981053));
#63907=CARTESIAN_POINT('Ctrl Pts',(47.031728186425,2.09862348765025,339.45014634984));
#63908=CARTESIAN_POINT('Ctrl Pts',(47.0239710766503,2.22198183952132,339.389848548055));
#63909=CARTESIAN_POINT('Ctrl Pts',(47.0162139668755,2.34251332956389,339.324559441529));
#63910=CARTESIAN_POINT('Ctrl Pts',(47.0084527119494,2.46310922778097,339.259235446592));
#63911=CARTESIAN_POINT('Ctrl Pts',(47.0006914570232,2.58087491876656,339.18891503258));
#63912=CARTESIAN_POINT('Ctrl Pts',(46.992930202097,2.69538491084248,339.113889065702));
#63913=CARTESIAN_POINT('Ctrl Pts',(46.9851565316924,2.81007808158692,339.038743081728));
#63914=CARTESIAN_POINT('Ctrl Pts',(46.9773828612877,2.9215048283188,338.958876730843));
#63915=CARTESIAN_POINT('Ctrl Pts',(46.969609190883,3.02927118029817,338.874622456281));
#63916=CARTESIAN_POINT('Ctrl Pts',(46.9621973867059,3.13202098266611,338.794290238469));
#63917=CARTESIAN_POINT('Ctrl Pts',(46.9547855825288,3.23144328444129,338.709969605433));
#63918=CARTESIAN_POINT('Ctrl Pts',(46.9473737783517,3.32722849521764,338.62197923836));
#63919=CARTESIAN_POINT('Ctrl Pts',(46.9395986995733,3.4277084245034,338.529676201287));
#63920=CARTESIAN_POINT('Ctrl Pts',(46.9318236207949,3.5245032537523,338.433042910573));
#63921=CARTESIAN_POINT('Ctrl Pts',(46.9240485420164,3.61721689129453,338.332405291052));
#63922=CARTESIAN_POINT('Ctrl Pts',(46.9162830309674,3.70981643880332,338.231891512529));
#63923=CARTESIAN_POINT('Ctrl Pts',(46.9085175199184,3.79834452496752,338.1273834944));
#63924=CARTESIAN_POINT('Ctrl Pts',(46.9007520088694,3.88243930488574,338.019246281173));
#63925=CARTESIAN_POINT('Ctrl Pts',(46.8929941973472,3.96645070458483,337.911216286309));
#63926=CARTESIAN_POINT('Ctrl Pts',(46.885236385825,4.04603730719556,337.799564563848));
#63927=CARTESIAN_POINT('Ctrl Pts',(46.8774785743028,4.12087547659111,337.684691484869));
#63928=CARTESIAN_POINT('Ctrl Pts',(46.8697266007797,4.19565732789087,337.569904851525));
#63929=CARTESIAN_POINT('Ctrl Pts',(46.8619746272568,4.26569764604235,337.451902013046));
#63930=CARTESIAN_POINT('Ctrl Pts',(46.8542226537338,4.33071453580504,337.331114469919));
#63931=CARTESIAN_POINT('Ctrl Pts',(46.8464739631761,4.39570389087636,337.210378080389));
#63932=CARTESIAN_POINT('Ctrl Pts',(46.8387252726185,4.45567386397908,337.086859675268));
#63933=CARTESIAN_POINT('Ctrl Pts',(46.8309765820609,4.51038729987976,336.961017457236));
#63934=CARTESIAN_POINT('Ctrl Pts',(46.823229503683,4.56508935219312,336.835201421728));
#63935=CARTESIAN_POINT('Ctrl Pts',(46.8154824253052,4.61453688693182,336.707062893235));
#63936=CARTESIAN_POINT('Ctrl Pts',(46.8077353469274,4.65854008662604,336.577081901424));
#63937=CARTESIAN_POINT('Ctrl Pts',(46.7999882036216,4.70254365510943,336.447099820246));
#63938=CARTESIAN_POINT('Ctrl Pts',(46.7922410603157,4.74110267220092,336.315275615184));
#63939=CARTESIAN_POINT('Ctrl Pts',(46.7844939170099,4.77407671003051,336.182106014385));
#63940=CARTESIAN_POINT('Ctrl Pts',(46.7767450319818,4.80705816112386,336.048906474232));
#63941=CARTESIAN_POINT('Ctrl Pts',(46.7689961469537,4.83445204047934,335.914361315796));
#63942=CARTESIAN_POINT('Ctrl Pts',(46.7612472619256,4.85616879177119,335.778978644333));
#63943=CARTESIAN_POINT('Ctrl Pts',(46.7534901521509,4.87790859344723,335.643452276305));
#63944=CARTESIAN_POINT('Ctrl Pts',(46.7457330423761,4.89395916802745,335.507087006048));
#63945=CARTESIAN_POINT('Ctrl Pts',(46.7379759326014,4.90428267082493,335.370397822815));
#63946=CARTESIAN_POINT('Ctrl Pts',(46.7302146776752,4.91461169017222,335.233635597253));
#63947=CARTESIAN_POINT('Ctrl Pts',(46.7224534227491,4.91920752659564,335.096549504276));
#63948=CARTESIAN_POINT('Ctrl Pts',(46.7146921678229,4.91808451773345,334.959654753309));
#63949=CARTESIAN_POINT('Ctrl Pts',(46.7069184974182,4.91695971242307,334.822541015355));
#63950=CARTESIAN_POINT('Ctrl Pts',(46.6991448270135,4.91009780041177,334.685619621648));
#63951=CARTESIAN_POINT('Ctrl Pts',(46.6913711566089,4.89756514013403,334.5494017747));
#63952=CARTESIAN_POINT('Ctrl Pts',(46.6839593524318,4.88561587820755,334.4195249013));
#63953=CARTESIAN_POINT('Ctrl Pts',(46.6765475482549,4.86851197132704,334.290287833804));
#63954=CARTESIAN_POINT('Ctrl Pts',(46.6691357440779,4.84635386816852,334.162123370067));
#63955=CARTESIAN_POINT('Ctrl Pts',(46.6613606652994,4.82310973036836,334.027677184178));
#63956=CARTESIAN_POINT('Ctrl Pts',(46.653585586521,4.79422997081942,333.893986528814));
#63957=CARTESIAN_POINT('Ctrl Pts',(46.6458105077426,4.75977431873624,333.761560862537));
#63958=CARTESIAN_POINT('Ctrl Pts',(46.6380449966936,4.72536106652648,333.629298154474));
#63959=CARTESIAN_POINT('Ctrl Pts',(46.6302794856445,4.68538567166479,333.498297712876));
#63960=CARTESIAN_POINT('Ctrl Pts',(46.6225139745955,4.63995929282773,333.369061367371));
#63961=CARTESIAN_POINT('Ctrl Pts',(46.6147561630733,4.59457795437758,333.239953160079));
#63962=CARTESIAN_POINT('Ctrl Pts',(46.6069983515511,4.54375651632663,333.11260593444));
#63963=CARTESIAN_POINT('Ctrl Pts',(46.5992405400289,4.48765652117703,332.987508506742));
#63964=CARTESIAN_POINT('Ctrl Pts',(46.5914885665059,4.43159874305277,332.862505218825));
#63965=CARTESIAN_POINT('Ctrl Pts',(46.5837365929829,4.37027047375947,332.739748714144));
#63966=CARTESIAN_POINT('Ctrl Pts',(46.5759846194599,4.3038820215742,332.619709554094));
#63967=CARTESIAN_POINT('Ctrl Pts',(46.5682359289023,4.23752168493788,332.4997212307));
#63968=CARTESIAN_POINT('Ctrl Pts',(46.5604872383447,4.16610561644475,332.38244830442));
#63969=CARTESIAN_POINT('Ctrl Pts',(46.552738547787,4.08989079019746,332.268338163909));
#63970=CARTESIAN_POINT('Ctrl Pts',(46.5449914694092,4.01369182108139,332.154251764965));
#63971=CARTESIAN_POINT('Ctrl Pts',(46.5372443910314,3.93269629710292,332.043327167733));
#63972=CARTESIAN_POINT('Ctrl Pts',(46.5294973126536,3.84720516432347,331.935983765366));
#63973=CARTESIAN_POINT('Ctrl Pts',(46.5217501693478,3.76171331504598,331.828639463358));
#63974=CARTESIAN_POINT('Ctrl Pts',(46.514003026042,3.67172602532727,331.724876721834));
#63975=CARTESIAN_POINT('Ctrl Pts',(46.5062558827362,3.57758501088609,331.625082437691));
#63976=CARTESIAN_POINT('Ctrl Pts',(46.4985069977081,3.48342283154625,331.525265717673));
#63977=CARTESIAN_POINT('Ctrl Pts',(46.49075811268,3.3851053374024,331.429419514672));
#63978=CARTESIAN_POINT('Ctrl Pts',(46.4830092276519,3.28301134093816,331.337894103419));
#63979=CARTESIAN_POINT('Ctrl Pts',(46.4752521178772,3.18080898085117,331.24627154615));
#63980=CARTESIAN_POINT('Ctrl Pts',(46.4674950081024,3.0748224027545,331.158979203188));
#63981=CARTESIAN_POINT('Ctrl Pts',(46.4597378983277,2.96546419216445,331.076327589172));
#63982=CARTESIAN_POINT('Ctrl Pts',(46.4519766434016,2.85604754404326,330.993631808777));
#63983=CARTESIAN_POINT('Ctrl Pts',(46.4442153884754,2.74325599465342,330.915581920972));
#63984=CARTESIAN_POINT('Ctrl Pts',(46.4364541335492,2.62753055351063,330.842444678315));
#63985=CARTESIAN_POINT('Ctrl Pts',(46.4286804631446,2.51161998937685,330.769190439906));
#63986=CARTESIAN_POINT('Ctrl Pts',(46.4209067927399,2.39276649399367,330.700864745426));
#63987=CARTESIAN_POINT('Ctrl Pts',(46.4131331223353,2.27143585881414,330.637688433663));
#63988=CARTESIAN_POINT('Ctrl Pts',(46.4057213181582,2.1557531938922,330.577452994413));
#63989=CARTESIAN_POINT('Ctrl Pts',(46.398309513981,2.03781908124668,330.52189844176));
#63990=CARTESIAN_POINT('Ctrl Pts',(46.3908977098039,1.91805182836833,330.471174518024));
#63991=CARTESIAN_POINT('Ctrl Pts',(46.3831226310255,1.79241442565861,330.417964463687));
#63992=CARTESIAN_POINT('Ctrl Pts',(46.375347552247,1.66436260638541,330.369902384829));
#63993=CARTESIAN_POINT('Ctrl Pts',(46.3675724734686,1.534357108029,330.327213751139));
#63994=CARTESIAN_POINT('Ctrl Pts',(46.3598069624196,1.40451158971479,330.284577648531));
#63995=CARTESIAN_POINT('Ctrl Pts',(46.3520414513706,1.27271754365588,330.247301955156));
#63996=CARTESIAN_POINT('Ctrl Pts',(46.3442759403216,1.13945712343001,330.215564764116));
#63997=CARTESIAN_POINT('Ctrl Pts',(46.3365181287993,1.00632883129877,330.183859040594));
#63998=CARTESIAN_POINT('Ctrl Pts',(46.3287603172772,0.871737436162197,330.157680981104));
#63999=CARTESIAN_POINT('Ctrl Pts',(46.321002505755,0.736181413981547,330.137159267649));
#64000=CARTESIAN_POINT('Ctrl Pts',(46.313250532232,0.600727402006408,330.116652997435));
#64001=CARTESIAN_POINT('Ctrl Pts',(46.3054985587089,0.464310592794973,330.101794659016));
#64002=CARTESIAN_POINT('Ctrl Pts',(46.2977465851859,0.327440501340161,330.092662047445));
#64003=CARTESIAN_POINT('Ctrl Pts',(46.2899978946283,0.190628374450339,330.083533303542));
#64004=CARTESIAN_POINT('Ctrl Pts',(46.2822492040707,0.0533637363179859,
330.080125489603));
#64005=CARTESIAN_POINT('Ctrl Pts',(46.2745005135131,-0.0838381309592026,
330.082464618297));
#64006=CARTESIAN_POINT('Ctrl Pts',(46.2667534351352,-0.221011452241972,
330.084803260316));
#64007=CARTESIAN_POINT('Ctrl Pts',(46.2590063567574,-0.358121638074713,
330.092886459979));
#64008=CARTESIAN_POINT('Ctrl Pts',(46.2512592783796,-0.494653152623377,
330.106688103023));
#64009=CARTESIAN_POINT('Ctrl Pts',(46.2435121350738,-0.631185811437452,
330.120489861737));
#64010=CARTESIAN_POINT('Ctrl Pts',(46.235764991768,-0.767139400401763,330.140010120114));
#64011=CARTESIAN_POINT('Ctrl Pts',(46.2280178484622,-0.902003647680204,
330.165170894223));
#64012=CARTESIAN_POINT('Ctrl Pts',(46.2202689634341,-1.03689821530477,330.190337325008));
#64013=CARTESIAN_POINT('Ctrl Pts',(46.212520078406,-1.17070256973624,330.221146723247));
#64014=CARTESIAN_POINT('Ctrl Pts',(46.2047711933779,-1.30291716030652,330.257470091198));
#64015=CARTESIAN_POINT('Ctrl Pts',(46.1970140836032,-1.43527208480926,330.293832013147));
#64016=CARTESIAN_POINT('Ctrl Pts',(46.1892569738284,-1.56603349722304,330.335719492183));
#64017=CARTESIAN_POINT('Ctrl Pts',(46.1814998640537,-1.6947170054669,330.382953613631));
#64018=CARTESIAN_POINT('Ctrl Pts',(46.1737386091275,-1.82346927806306,330.430212975483));
#64019=CARTESIAN_POINT('Ctrl Pts',(46.1659773542014,-1.95014107319188,330.482824522875));
#64020=CARTESIAN_POINT('Ctrl Pts',(46.1582160992752,-2.07426941738349,330.54056175661));
#64021=CARTESIAN_POINT('Ctrl Pts',(46.1504424288706,-2.19859632647247,330.598391351103));
#64022=CARTESIAN_POINT('Ctrl Pts',(46.1426687584659,-2.32037130678936,330.661362837188));
#64023=CARTESIAN_POINT('Ctrl Pts',(46.1348950880612,-2.43915658380393,330.729204029436));
#64024=CARTESIAN_POINT('Ctrl Pts',(46.1274832838841,-2.55241237759628,330.793887197863));
#64025=CARTESIAN_POINT('Ctrl Pts',(46.1200714797069,-2.66295030153696,330.862996753041));
#64026=CARTESIAN_POINT('Ctrl Pts',(46.1126596755298,-2.77041806393055,330.936261965438));
#64027=CARTESIAN_POINT('Ctrl Pts',(46.104918932011,-2.88265529596461,331.012778722283));
#64028=CARTESIAN_POINT('Ctrl Pts',(46.0971781884923,-2.99190525043291,331.094075106653));
#64029=CARTESIAN_POINT('Ctrl Pts',(46.0894374449736,-3.09773120365827,331.179889471183));
#64030=CARTESIAN_POINT('Ctrl Pts',(46.0817062475476,-3.20342664947599,331.265598007133));
#64031=CARTESIAN_POINT('Ctrl Pts',(46.0739750501217,-3.30570619071891,331.355813192939));
#64032=CARTESIAN_POINT('Ctrl Pts',(46.0662438526958,-3.40416116482187,331.450229609338));
#64033=CARTESIAN_POINT('Ctrl Pts',(46.0585202979289,-3.50251881146617,331.544552690586));
#64034=CARTESIAN_POINT('Ctrl Pts',(46.050796743162,-3.59705913062881,331.643068467432));
#64035=CARTESIAN_POINT('Ctrl Pts',(46.0430731883951,-3.68740604249248,331.745430943997));
#64036=CARTESIAN_POINT('Ctrl Pts',(46.0353553798691,-3.7776857372343,331.847717263992));
#64037=CARTESIAN_POINT('Ctrl Pts',(46.0276375713431,-3.86377797347314,331.953844293326));
#64038=CARTESIAN_POINT('Ctrl Pts',(46.0199197628172,-3.94534340329375,332.063429126926));
#64039=CARTESIAN_POINT('Ctrl Pts',(46.0122051006626,-4.02687558078156,332.172969285332));
#64040=CARTESIAN_POINT('Ctrl Pts',(46.004490438508,-4.10388438634641,332.285964128855));
#64041=CARTESIAN_POINT('Ctrl Pts',(45.9967757763534,-4.17607085085154,332.401997823102));
#64042=CARTESIAN_POINT('Ctrl Pts',(45.9890625812274,-4.24824358830057,332.518009452256));
#64043=CARTESIAN_POINT('Ctrl Pts',(45.9813493861013,-4.31559560005693,332.63705844786));
#64044=CARTESIAN_POINT('Ctrl Pts',(45.9736361909752,-4.37787160560738,332.758700540464));
#64045=CARTESIAN_POINT('Ctrl Pts',(45.9659227545427,-4.44014955945599,332.880346438628));
#64046=CARTESIAN_POINT('Ctrl Pts',(45.9582093181101,-4.49735101127524,333.004585243802));
#64047=CARTESIAN_POINT('Ctrl Pts',(45.9504958816776,-4.54926716230683,333.130949078153));
#64048=CARTESIAN_POINT('Ctrl Pts',(45.9427804957732,-4.60119643447799,333.257344849338));
#64049=CARTESIAN_POINT('Ctrl Pts',(45.9350651098687,-4.64783759855045,333.38586635311));
#64050=CARTESIAN_POINT('Ctrl Pts',(45.9273497239643,-4.68903058355568,333.516027207467));
#64051=CARTESIAN_POINT('Ctrl Pts',(45.9196261803307,-4.73026712324766,333.64632568514));
#64052=CARTESIAN_POINT('Ctrl Pts',(45.9119026366971,-4.7660438609636,333.778266598071));
#64053=CARTESIAN_POINT('Ctrl Pts',(45.9041790930635,-4.79625094802646,333.91134950234));
#64054=CARTESIAN_POINT('Ctrl Pts',(45.896451155459,-4.8264752200848,334.044508118282));
#64055=CARTESIAN_POINT('Ctrl Pts',(45.8887232178545,-4.8511234588629,334.178809631967));
#64056=CARTESIAN_POINT('Ctrl Pts',(45.8809952802499,-4.87013743076969,334.313746061639));
#64057=CARTESIAN_POINT('Ctrl Pts',(45.8732556814828,-4.8891800940337,334.448886105228));
#64058=CARTESIAN_POINT('Ctrl Pts',(45.8655160827156,-4.90257147075479,334.584662586107));
#64059=CARTESIAN_POINT('Ctrl Pts',(45.8577764839485,-4.91030537113275,334.720564453362));
#64060=CARTESIAN_POINT('Ctrl Pts',(45.8524567814796,-4.91562115689539,334.813974657239));
#64061=CARTESIAN_POINT('Ctrl Pts',(45.8471370790106,-4.91826527278068,334.907444081807));
#64062=CARTESIAN_POINT('Ctrl Pts',(45.8418173765417,-4.91824993362185,335.000808040044));
#64063=CARTESIAN_POINT('',(44.0918173765497,-4.91824794925201,334.995508655169));
#64064=CARTESIAN_POINT('Ctrl Pts',(45.8418173765086,-4.91824993362175,335.000808040625));
#64065=CARTESIAN_POINT('Ctrl Pts',(45.8393521314244,-4.91824282517663,335.044074565478));
#64066=CARTESIAN_POINT('Ctrl Pts',(45.8368868863402,-4.91766479712218,335.08733580685));
#64067=CARTESIAN_POINT('Ctrl Pts',(45.8344216412559,-4.91651619026007,335.130581826494));
#64068=CARTESIAN_POINT('Ctrl Pts',(45.8266465624775,-4.91289362595788,335.266974435788));
#64069=CARTESIAN_POINT('Ctrl Pts',(45.8188714836991,-4.90358538870505,335.403431713215));
#64070=CARTESIAN_POINT('Ctrl Pts',(45.8110964049206,-4.88857715149386,335.539440910937));
#64071=CARTESIAN_POINT('Ctrl Pts',(45.8033308938716,-4.87358738287399,335.675282740682));
#64072=CARTESIAN_POINT('Ctrl Pts',(45.7955653828226,-4.85291161302988,335.810677203031));
#64073=CARTESIAN_POINT('Ctrl Pts',(45.7877998717736,-4.82658750698835,335.94511168646));
#64074=CARTESIAN_POINT('Ctrl Pts',(45.7800420602514,-4.80028950137461,336.079412877708));
#64075=CARTESIAN_POINT('Ctrl Pts',(45.7722842487292,-4.76835437918846,336.212755603099));
#64076=CARTESIAN_POINT('Ctrl Pts',(45.764526437207,-4.73087153887271,336.344632866319));
#64077=CARTESIAN_POINT('Ctrl Pts',(45.7567744636839,-4.69341690558295,336.476410887716));
#64078=CARTESIAN_POINT('Ctrl Pts',(45.7490224901609,-4.65042297039963,336.606725267558));
#64079=CARTESIAN_POINT('Ctrl Pts',(45.7412705166379,-4.60203001953569,336.73508004478));
#64080=CARTESIAN_POINT('Ctrl Pts',(45.7335218260803,-4.55365756311524,336.863380463677));
#64081=CARTESIAN_POINT('Ctrl Pts',(45.7257731355226,-4.49989077628166,336.989722565571));
#64082=CARTESIAN_POINT('Ctrl Pts',(45.718024444965,-4.44091946384773,337.113626593824));
#64083=CARTESIAN_POINT('Ctrl Pts',(45.7102773665872,-4.38196042088796,337.237504842808));
#64084=CARTESIAN_POINT('Ctrl Pts',(45.7025302882094,-4.31779917405665,337.358945674413));
#64085=CARTESIAN_POINT('Ctrl Pts',(45.6947832098316,-4.24867307617483,337.477490697114));
#64086=CARTESIAN_POINT('Ctrl Pts',(45.6870360665258,-4.17954639894964,337.596036713337));
#64087=CARTESIAN_POINT('Ctrl Pts',(45.67928892322,-4.10545498457594,337.711686534588));
#64088=CARTESIAN_POINT('Ctrl Pts',(45.6715417799142,-4.02668121375347,337.824008049795));
#64089=CARTESIAN_POINT('Ctrl Pts',(45.6637928948861,-3.94788973291502,337.936354817262));
#64090=CARTESIAN_POINT('Ctrl Pts',(45.656044009858,-3.86441402527817,338.045371469748));
#64091=CARTESIAN_POINT('Ctrl Pts',(45.6482951248299,-3.77657845958326,338.150656788848));
#64092=CARTESIAN_POINT('Ctrl Pts',(45.6405380150551,-3.68864966431141,338.256053858873));
#64093=CARTESIAN_POINT('Ctrl Pts',(45.6327809052804,-3.5963520177112,338.357711383476));
#64094=CARTESIAN_POINT('Ctrl Pts',(45.6250237955057,-3.50004903983596,338.455262621168));
#64095=CARTESIAN_POINT('Ctrl Pts',(45.6172625405795,-3.40369460072845,338.552865987123));
#64096=CARTESIAN_POINT('Ctrl Pts',(45.6095012856534,-3.30333085142551,338.646358427598));
#64097=CARTESIAN_POINT('Ctrl Pts',(45.6017400307272,-3.19935574695672,338.735412409215));
#64098=CARTESIAN_POINT('Ctrl Pts',(45.5939663603225,-3.0952143162062,338.82460884818));
#64099=CARTESIAN_POINT('Ctrl Pts',(45.5861926899179,-2.98745029356408,338.909352398465));
#64100=CARTESIAN_POINT('Ctrl Pts',(45.5784190195132,-2.8764927751468,338.989357388982));
#64101=CARTESIAN_POINT('Ctrl Pts',(45.5710072153362,-2.77070035590728,339.065638127943));
#64102=CARTESIAN_POINT('Ctrl Pts',(45.5635954111591,-2.66200530443199,339.137611380129));
#64103=CARTESIAN_POINT('Ctrl Pts',(45.5561836069821,-2.55079997644987,339.205068672762));
#64104=CARTESIAN_POINT('Ctrl Pts',(45.5484085282036,-2.43414414407918,339.275832248251));
#64105=CARTESIAN_POINT('Ctrl Pts',(45.5406334494252,-2.314357087019,339.341849615695));
#64106=CARTESIAN_POINT('Ctrl Pts',(45.5328583706467,-2.19186223269826,339.402831249931));
#64107=CARTESIAN_POINT('Ctrl Pts',(45.5250928595977,-2.06951811609416,339.463737842384));
#64108=CARTESIAN_POINT('Ctrl Pts',(45.5173273485488,-1.94447317875349,339.519620858933));
#64109=CARTESIAN_POINT('Ctrl Pts',(45.5095618374997,-1.81717886934789,339.570234569395));
#64110=CARTESIAN_POINT('Ctrl Pts',(45.5018040259775,-1.69001077262058,339.620798096216));
#64111=CARTESIAN_POINT('Ctrl Pts',(45.4940462144554,-1.56059810304602,339.666102570577));
#64112=CARTESIAN_POINT('Ctrl Pts',(45.4862884029332,-1.42941558326661,339.705948804738));
#64113=CARTESIAN_POINT('Ctrl Pts',(45.4785364294102,-1.29833178249355,339.745765053344));
#64114=CARTESIAN_POINT('Ctrl Pts',(45.4707844558872,-1.16548115503049,339.780131124383));
#64115=CARTESIAN_POINT('Ctrl Pts',(45.4630324823642,-1.03135668203651,339.808896594534));
#64116=CARTESIAN_POINT('Ctrl Pts',(45.4552837918066,-0.897289010836286,
339.837649882491));
#64117=CARTESIAN_POINT('Ctrl Pts',(45.4475351012489,-0.761948948469715,
339.860807205221));
#64118=CARTESIAN_POINT('Ctrl Pts',(45.4397864106913,-0.625842646804415,
339.878268549797));
#64119=CARTESIAN_POINT('Ctrl Pts',(45.4320393323134,-0.489764663192144,
339.895726261394));
#64120=CARTESIAN_POINT('Ctrl Pts',(45.4242922539356,-0.352921144837132,
339.907490302369));
#64121=CARTESIAN_POINT('Ctrl Pts',(45.4165451755578,-0.215826008181983,
339.913512205815));
#64122=CARTESIAN_POINT('Ctrl Pts',(45.408798032252,-0.0787297225375417,
339.919534159731));
#64123=CARTESIAN_POINT('Ctrl Pts',(45.4010508889462,0.058617795115445,339.919813862977));
#64124=CARTESIAN_POINT('Ctrl Pts',(45.3933037456404,0.195700360956632,339.914354935413));
#64125=CARTESIAN_POINT('Ctrl Pts',(45.3855548606123,0.33281374586878,339.908894780567));
#64126=CARTESIAN_POINT('Ctrl Pts',(45.3778059755842,0.469661669949456,339.897693443173));
#64127=CARTESIAN_POINT('Ctrl Pts',(45.3700570905561,0.605731205545558,339.880806569526));
#64128=CARTESIAN_POINT('Ctrl Pts',(45.3622999807814,0.741945166752789,339.863901771977));
#64129=CARTESIAN_POINT('Ctrl Pts',(45.3545428710067,0.877378700573073,339.841299431537));
#64130=CARTESIAN_POINT('Ctrl Pts',(45.346785761232,1.01152668470462,339.813106775112));
#64131=CARTESIAN_POINT('Ctrl Pts',(45.3390245063058,1.14574635322976,339.784899053433));
#64132=CARTESIAN_POINT('Ctrl Pts',(45.3312632513797,1.27867872461738,339.751095159613));
#64133=CARTESIAN_POINT('Ctrl Pts',(45.3235019964535,1.40983301276093,339.711852495424));
#64134=CARTESIAN_POINT('Ctrl Pts',(45.3157283260488,1.54119710502226,339.67254705576));
#64135=CARTESIAN_POINT('Ctrl Pts',(45.3079546556442,1.67077706053139,339.627785587719));
#64136=CARTESIAN_POINT('Ctrl Pts',(45.3001809852395,1.79810044384551,339.577774334362));
#64137=CARTESIAN_POINT('Ctrl Pts',(45.2927691810624,1.91949689303481,339.53009111688));
#64138=CARTESIAN_POINT('Ctrl Pts',(45.2853573768853,2.03884186555602,339.477635985769));
#64139=CARTESIAN_POINT('Ctrl Pts',(45.2779455727082,2.15574772600152,339.420626064749));
#64140=CARTESIAN_POINT('Ctrl Pts',(45.2701704939297,2.27838349091159,339.360821917676));
#64141=CARTESIAN_POINT('Ctrl Pts',(45.2623954151513,2.39872255356924,339.295816211449));
#64142=CARTESIAN_POINT('Ctrl Pts',(45.2546203363729,2.51629230521065,339.225808336548));
#64143=CARTESIAN_POINT('Ctrl Pts',(45.2468548253238,2.63371737978781,339.155886610794));
#64144=CARTESIAN_POINT('Ctrl Pts',(45.2390893142748,2.74837959128799,339.080975162089));
#64145=CARTESIAN_POINT('Ctrl Pts',(45.2313238032258,2.85982799517733,339.00132064455));
#64146=CARTESIAN_POINT('Ctrl Pts',(45.2235659917036,2.97116589764981,338.921745104697));
#64147=CARTESIAN_POINT('Ctrl Pts',(45.2158081801814,3.0792960178723,338.8374360806));
#64148=CARTESIAN_POINT('Ctrl Pts',(45.2080503686592,3.18379395496485,338.748684984742));
#64149=CARTESIAN_POINT('Ctrl Pts',(45.2002983951362,3.28821325404591,338.660000676898));
#64150=CARTESIAN_POINT('Ctrl Pts',(45.1925464216132,3.38900551383834,338.566881202984));
#64151=CARTESIAN_POINT('Ctrl Pts',(45.1847944480901,3.4857774597702,338.469659718684));
#64152=CARTESIAN_POINT('Ctrl Pts',(45.1770457575325,3.58250842272536,338.37247940774));
#64153=CARTESIAN_POINT('Ctrl Pts',(45.1692970669749,3.6752221830072,338.271200818039));
#64154=CARTESIAN_POINT('Ctrl Pts',(45.1615483764173,3.76356072979137,338.16619546075));
#64155=CARTESIAN_POINT('Ctrl Pts',(45.1538012980394,3.85188089700307,338.061211950702));
#64156=CARTESIAN_POINT('Ctrl Pts',(45.1460542196616,3.93582740989455,337.95250351428));
#64157=CARTESIAN_POINT('Ctrl Pts',(45.1383071412838,4.01508140193562,337.840476086562));
#64158=CARTESIAN_POINT('Ctrl Pts',(45.130559997978,4.09433605820147,337.728447719946));
#64159=CARTESIAN_POINT('Ctrl Pts',(45.1228128546722,4.16889788942985,337.613100625647));
#64160=CARTESIAN_POINT('Ctrl Pts',(45.1150657113664,4.23849060295287,337.494870832564));
#64161=CARTESIAN_POINT('Ctrl Pts',(45.1073168263383,4.30809896239539,337.376614458914));
#64162=CARTESIAN_POINT('Ctrl Pts',(45.0995679413101,4.3727357828634,337.255474433636));
#64163=CARTESIAN_POINT('Ctrl Pts',(45.091819056282,4.43217028392748,337.131912201938));
#64164=CARTESIAN_POINT('Ctrl Pts',(45.0840619465073,4.49166786938506,337.00821882001));
#64165=CARTESIAN_POINT('Ctrl Pts',(45.0763048367326,4.54595193543428,336.882098448739));
#64166=CARTESIAN_POINT('Ctrl Pts',(45.0685477269579,4.59483930080565,336.754033882875));
#64167=CARTESIAN_POINT('Ctrl Pts',(45.0607864720317,4.64375279002193,336.625900883401));
#64168=CARTESIAN_POINT('Ctrl Pts',(45.0530252171055,4.68726370835036,336.495821989701));
#64169=CARTESIAN_POINT('Ctrl Pts',(45.0452639621793,4.72523882577344,336.36429509341));
#64170=CARTESIAN_POINT('Ctrl Pts',(45.0374902917747,4.76327469100834,336.23255779695));
#64171=CARTESIAN_POINT('Ctrl Pts',(45.02971662137,4.79575696681091,336.099368249126));
#64172=CARTESIAN_POINT('Ctrl Pts',(45.0219429509654,4.82260342544471,335.965235340934));
#64173=CARTESIAN_POINT('Ctrl Pts',(45.0145311467884,4.84820017496996,335.837346351891));
#64174=CARTESIAN_POINT('Ctrl Pts',(45.0071193426114,4.86867394878192,335.708600137068));
#64175=CARTESIAN_POINT('Ctrl Pts',(44.9997075384343,4.88399755908635,335.579440165452));
#64176=CARTESIAN_POINT('Ctrl Pts',(44.9919324596559,4.90007222517866,335.443949678877));
#64177=CARTESIAN_POINT('Ctrl Pts',(44.9841573808775,4.91052991183441,335.307575676101));
#64178=CARTESIAN_POINT('Ctrl Pts',(44.976382302099,4.91528253504174,335.170823485545));
#64179=CARTESIAN_POINT('Ctrl Pts',(44.96861679105,4.92002930984365,335.034239577265));
#64180=CARTESIAN_POINT('Ctrl Pts',(44.960851280001,4.91908497642098,334.897278794092));
#64181=CARTESIAN_POINT('Ctrl Pts',(44.953085768952,4.91241291952042,334.760453823598));
#64182=CARTESIAN_POINT('Ctrl Pts',(44.9453279574298,4.90574747798371,334.623764515461));
#64183=CARTESIAN_POINT('Ctrl Pts',(44.9375701459076,4.89336563352381,334.487211139922));
#64184=CARTESIAN_POINT('Ctrl Pts',(44.9298123343854,4.8752827734466,334.351308284749));
#64185=CARTESIAN_POINT('Ctrl Pts',(44.9220603608624,4.85721352129504,334.215507700786));
#64186=CARTESIAN_POINT('Ctrl Pts',(44.9143083873394,4.83345184429638,334.080357048689));
#64187=CARTESIAN_POINT('Ctrl Pts',(44.9065564138164,4.80406507673578,333.946367331093));
#64188=CARTESIAN_POINT('Ctrl Pts',(44.8988077232587,4.77469075448868,333.812434358223));
#64189=CARTESIAN_POINT('Ctrl Pts',(44.8910590327011,4.73969616332807,333.679661722989));
#64190=CARTESIAN_POINT('Ctrl Pts',(44.8833103421435,4.69919997472217,333.548551530342));
#64191=CARTESIAN_POINT('Ctrl Pts',(44.8755632637656,4.65871221168655,333.417468616267));
#64192=CARTESIAN_POINT('Ctrl Pts',(44.8678161853878,4.61272524328237,333.288047830019));
#64193=CARTESIAN_POINT('Ctrl Pts',(44.8600691070099,4.56140787200017,333.160776988031));
#64194=CARTESIAN_POINT('Ctrl Pts',(44.8523219637041,4.51009007062896,333.033505079391));
#64195=CARTESIAN_POINT('Ctrl Pts',(44.8445748203984,4.45344192344516,332.908383513464));
#64196=CARTESIAN_POINT('Ctrl Pts',(44.8368276770925,4.3916805786366,332.785880590906));
#64197=CARTESIAN_POINT('Ctrl Pts',(44.8290787920645,4.32990534856658,332.663350127091));
#64198=CARTESIAN_POINT('Ctrl Pts',(44.8213299070363,4.26301480931614,332.543439827102));
#64199=CARTESIAN_POINT('Ctrl Pts',(44.8135810220082,4.19127211147331,332.426593473606));
#64200=CARTESIAN_POINT('Ctrl Pts',(44.8058239122335,4.11945326518965,332.309623098184));
#64201=CARTESIAN_POINT('Ctrl Pts',(44.7980668024588,4.04277217728585,332.195723499263));
#64202=CARTESIAN_POINT('Ctrl Pts',(44.790309692684,3.96153571027199,332.085309985824));
#64203=CARTESIAN_POINT('Ctrl Pts',(44.7825484377578,3.88025583308765,331.974837470933));
#64204=CARTESIAN_POINT('Ctrl Pts',(44.7747871828317,3.7944159708271,331.867855058139));
#64205=CARTESIAN_POINT('Ctrl Pts',(44.7670259279055,3.70436271278245,331.76474422114));
#64206=CARTESIAN_POINT('Ctrl Pts',(44.7592522575008,3.61416539887323,331.661468440405));
#64207=CARTESIAN_POINT('Ctrl Pts',(44.7514785870963,3.51974148990276,331.562076894961));
#64208=CARTESIAN_POINT('Ctrl Pts',(44.7437049166916,3.42147442502101,331.466914121985));
#64209=CARTESIAN_POINT('Ctrl Pts',(44.7362931125145,3.32778171565066,331.376181198985));
#64210=CARTESIAN_POINT('Ctrl Pts',(44.7288813083373,3.23059581071873,331.2892924015));
#64211=CARTESIAN_POINT('Ctrl Pts',(44.7214695041601,3.13027491988188,331.206510578839));
#64212=CARTESIAN_POINT('Ctrl Pts',(44.7136944253817,3.02503700334512,331.119671372456));
#64213=CARTESIAN_POINT('Ctrl Pts',(44.7059193466033,2.91601644931012,331.037077482602));
#64214=CARTESIAN_POINT('Ctrl Pts',(44.6981442678248,2.80359053191454,330.959076443205));
#64215=CARTESIAN_POINT('Ctrl Pts',(44.6903787567758,2.69130296176771,330.881171389053));
#64216=CARTESIAN_POINT('Ctrl Pts',(44.6826132457268,2.57561868426577,330.807848160592));
#64217=CARTESIAN_POINT('Ctrl Pts',(44.6748477346778,2.45694901471351,330.739414993032));
#64218=CARTESIAN_POINT('Ctrl Pts',(44.6670899231556,2.33839700648403,330.671049677158));
#64219=CARTESIAN_POINT('Ctrl Pts',(44.6593321116334,2.21686583324678,330.607564967384));
#64220=CARTESIAN_POINT('Ctrl Pts',(44.6515743001112,2.09279654978999,330.549226397166));
#64221=CARTESIAN_POINT('Ctrl Pts',(44.6438223265881,1.96882063240347,330.490931728572));
#64222=CARTESIAN_POINT('Ctrl Pts',(44.6360703530651,1.8423107588735,330.437775656901));
#64223=CARTESIAN_POINT('Ctrl Pts',(44.6283183795421,1.7137330806627,330.389978092162));
#64224=CARTESIAN_POINT('Ctrl Pts',(44.6205696889845,1.58520985517514,330.342200769721));
#64225=CARTESIAN_POINT('Ctrl Pts',(44.6128209984268,1.45462093236078,330.299777576588));
#64226=CARTESIAN_POINT('Ctrl Pts',(44.6050723078692,1.3224527629256,330.262880437193));
#64227=CARTESIAN_POINT('Ctrl Pts',(44.5973252294914,1.19031209218196,330.225990974556));
#64228=CARTESIAN_POINT('Ctrl Pts',(44.5895781511136,1.05659320462003,330.194625383774));
#64229=CARTESIAN_POINT('Ctrl Pts',(44.5818310727357,0.921797664197005,330.168905700695));
#64230=CARTESIAN_POINT('Ctrl Pts',(44.5740839294299,0.787000994057517,330.143185802059));
#64231=CARTESIAN_POINT('Ctrl Pts',(44.5663367861241,0.651128037006763,330.123111978764));
#64232=CARTESIAN_POINT('Ctrl Pts',(44.5585896428183,0.514690108401413,330.108755050622));
#64233=CARTESIAN_POINT('Ctrl Pts',(44.5508407577902,0.378221505653054,330.094394894738));
#64234=CARTESIAN_POINT('Ctrl Pts',(44.5430918727621,0.241188067251386,330.085754232465));
#64235=CARTESIAN_POINT('Ctrl Pts',(44.535342987734,0.104105385391348,330.082851931126));
#64236=CARTESIAN_POINT('Ctrl Pts',(44.5275858779592,-0.0331227974435458,
330.079946549254));
#64237=CARTESIAN_POINT('Ctrl Pts',(44.5198287681845,-0.170399936742121,
330.082791703458));
#64238=CARTESIAN_POINT('Ctrl Pts',(44.5120716584098,-0.307210729410955,
330.091354094026));
#64239=CARTESIAN_POINT('Ctrl Pts',(44.5043104034836,-0.444094629393122,
330.099921060062));
#64240=CARTESIAN_POINT('Ctrl Pts',(44.4965491485574,-0.580511297640694,
330.114211309338));
#64241=CARTESIAN_POINT('Ctrl Pts',(44.4887878936312,-0.71595238542965,330.134139824831));
#64242=CARTESIAN_POINT('Ctrl Pts',(44.4810142232266,-0.851610134818735,
330.154100219454));
#64243=CARTESIAN_POINT('Ctrl Pts',(44.4732405528219,-0.986288800994723,
330.179716830628));
#64244=CARTESIAN_POINT('Ctrl Pts',(44.4654668824172,-1.11949115436959,330.210853665027));
#64245=CARTESIAN_POINT('Ctrl Pts',(44.4580550782402,-1.24649290614678,330.240541072293));
#64246=CARTESIAN_POINT('Ctrl Pts',(44.4506432740633,-1.37215241932634,330.275246259122));
#64247=CARTESIAN_POINT('Ctrl Pts',(44.4432314698863,-1.4960548105155,330.314810242217));
#64248=CARTESIAN_POINT('Ctrl Pts',(44.4354563911078,-1.62603002698441,330.356313373979));
#64249=CARTESIAN_POINT('Ctrl Pts',(44.4276813123294,-1.75448226841276,330.403294790682));
#64250=CARTESIAN_POINT('Ctrl Pts',(44.419906233551,-1.88091512142092,330.455625305005));
#64251=CARTESIAN_POINT('Ctrl Pts',(44.412140722502,-2.00719239075435,330.507891423299));
#64252=CARTESIAN_POINT('Ctrl Pts',(44.4043752114529,-2.13145485836897,330.56549339406));
#64253=CARTESIAN_POINT('Ctrl Pts',(44.3966097004039,-2.25322073638608,330.628252137232));
#64254=CARTESIAN_POINT('Ctrl Pts',(44.3888518888817,-2.37486588318055,330.690948654927));
#64255=CARTESIAN_POINT('Ctrl Pts',(44.3810940773596,-2.49401902131213,330.758791592045));
#64256=CARTESIAN_POINT('Ctrl Pts',(44.3733362658374,-2.61021817797946,330.831553751595));
#64257=CARTESIAN_POINT('Ctrl Pts',(44.3655842923144,-2.72632989109651,330.904261155311));
#64258=CARTESIAN_POINT('Ctrl Pts',(44.3578323187914,-2.83949171750165,330.981880206456));
#64259=CARTESIAN_POINT('Ctrl Pts',(44.3500803452684,-2.94926646887166,331.064137914244));
#64260=CARTESIAN_POINT('Ctrl Pts',(44.3423316547108,-3.05899473056944,331.146360785844));
#64261=CARTESIAN_POINT('Ctrl Pts',(44.3345829641532,-3.16533845806015,331.233218172985));
#64262=CARTESIAN_POINT('Ctrl Pts',(44.3268342735956,-3.26788983003292,331.324394047063));
#64263=CARTESIAN_POINT('Ctrl Pts',(44.3190871952177,-3.37041986533623,331.415550951239));
#64264=CARTESIAN_POINT('Ctrl Pts',(44.3113401168399,-3.46915882262787,331.511024295628));
#64265=CARTESIAN_POINT('Ctrl Pts',(44.3035930384621,-3.56373265432442,331.610458344997));
#64266=CARTESIAN_POINT('Ctrl Pts',(44.2958458951563,-3.65830727864065,331.709893227719));
#64267=CARTESIAN_POINT('Ctrl Pts',(44.2880987518504,-3.74871643835432,331.813288598404));
#64268=CARTESIAN_POINT('Ctrl Pts',(44.2803516085446,-3.83462387749575,331.920252805726));
#64269=CARTESIAN_POINT('Ctrl Pts',(44.2726027235165,-3.92055063045348,332.027241060872));
#64270=CARTESIAN_POINT('Ctrl Pts',(44.2648538384884,-4.00197340419532,332.137799444548));
#64271=CARTESIAN_POINT('Ctrl Pts',(44.2571049534603,-4.07859731626657,332.251504594466));
#64272=CARTESIAN_POINT('Ctrl Pts',(44.2493478436856,-4.15530255774978,332.365330432205));
#64273=CARTESIAN_POINT('Ctrl Pts',(44.2415907339108,-4.22719854391608,332.482309383515));
#64274=CARTESIAN_POINT('Ctrl Pts',(44.2338336241361,-4.29403441713169,332.601990098647));
#64275=CARTESIAN_POINT('Ctrl Pts',(44.22607236921,-4.3609060053008,332.721734767326));
#64276=CARTESIAN_POINT('Ctrl Pts',(44.2183111142838,-4.42271191659104,332.844183727834));
#64277=CARTESIAN_POINT('Ctrl Pts',(44.2105498593577,-4.4792485469673,332.968863491296));
#64278=CARTESIAN_POINT('Ctrl Pts',(44.202776188953,-4.535875617527,333.093742701746));
#64279=CARTESIAN_POINT('Ctrl Pts',(44.1950025185483,-4.58721641681267,333.220859483564));
#64280=CARTESIAN_POINT('Ctrl Pts',(44.1872288481436,-4.63311622505206,333.349722111989));
#64281=CARTESIAN_POINT('Ctrl Pts',(44.1798170439665,-4.67687938617506,333.472586154058));
#64282=CARTESIAN_POINT('Ctrl Pts',(44.1724052397894,-4.71569662709086,333.597036887497));
#64283=CARTESIAN_POINT('Ctrl Pts',(44.1649934356124,-4.74947712303642,333.722639393024));
#64284=CARTESIAN_POINT('Ctrl Pts',(44.1550194885169,-4.79493499960332,333.891660688684));
#64285=CARTESIAN_POINT('Ctrl Pts',(44.1450455414214,-4.83139011897056,334.063198460588));
#64286=CARTESIAN_POINT('Ctrl Pts',(44.1350715943259,-4.85861284657801,334.236413548073));
#64287=CARTESIAN_POINT('Ctrl Pts',(44.125280948658,-4.88533527427563,334.406445284722));
#64288=CARTESIAN_POINT('Ctrl Pts',(44.1154903029901,-4.90316156846626,334.578093430656));
#64289=CARTESIAN_POINT('Ctrl Pts',(44.1056996573222,-4.91191959658431,334.750542710688));
#64290=CARTESIAN_POINT('Ctrl Pts',(44.101072230398,-4.91605896966456,334.832048718416));
#64291=CARTESIAN_POINT('Ctrl Pts',(44.0964448034738,-4.9181732720366,334.91373335727));
#64292=CARTESIAN_POINT('Ctrl Pts',(44.0918173765497,-4.91824794925201,334.995508655169));
#64293=CARTESIAN_POINT('',(42.3418173764774,-4.91824979877521,335.001406892883));
#64294=CARTESIAN_POINT('Ctrl Pts',(44.0918173765087,-4.91824794925267,334.995508655893));
#64295=CARTESIAN_POINT('Ctrl Pts',(44.0841435815425,-4.9183717886037,335.131118980953));
#64296=CARTESIAN_POINT('Ctrl Pts',(44.0764697865763,-4.9128826557159,335.266862873519));
#64297=CARTESIAN_POINT('Ctrl Pts',(44.0687959916102,-4.90177426318535,335.402233931032));
#64298=CARTESIAN_POINT('Ctrl Pts',(44.0611261793002,-4.89067163584767,335.537534731733));
#64299=CARTESIAN_POINT('Ctrl Pts',(44.0534563669902,-4.87395558128148,335.672462684876));
#64300=CARTESIAN_POINT('Ctrl Pts',(44.0457865546802,-4.85167188648578,335.806512844525));
#64301=CARTESIAN_POINT('Ctrl Pts',(44.0381187493999,-4.82939402286746,335.940527926047));
#64302=CARTESIAN_POINT('Ctrl Pts',(44.0304509441195,-4.80155148122578,336.073665276805));
#64303=CARTESIAN_POINT('Ctrl Pts',(44.0227831388392,-4.76824169222321,336.205426989512));
#64304=CARTESIAN_POINT('Ctrl Pts',(44.0151155972268,-4.73493304862312,336.337184171413));
#64305=CARTESIAN_POINT('Ctrl Pts',(44.0074480556143,-4.69615762947972,336.467565421799));
#64306=CARTESIAN_POINT('Ctrl Pts',(43.9997805140019,-4.65206345607596,336.596085418498));
#64307=CARTESIAN_POINT('Ctrl Pts',(43.9921114931604,-4.6079607759841,336.724630209393));
#64308=CARTESIAN_POINT('Ctrl Pts',(43.9844424723189,-4.55853743080427,336.851312654494));
#64309=CARTESIAN_POINT('Ctrl Pts',(43.9767734514774,-4.50399036886354,336.975665411876));
#64310=CARTESIAN_POINT('Ctrl Pts',(43.9690964997169,-4.44938689707111,337.10014676868));
#64311=CARTESIAN_POINT('Ctrl Pts',(43.9614195479563,-4.38964928656962,337.222293259315));
#64312=CARTESIAN_POINT('Ctrl Pts',(43.9537425961958,-4.3250216222201,337.341659887735));
#64313=CARTESIAN_POINT('Ctrl Pts',(43.9460616123199,-4.26036001390261,337.461089210314));
#64314=CARTESIAN_POINT('Ctrl Pts',(43.9383806284439,-4.19080344141514,337.577735420031));
#64315=CARTESIAN_POINT('Ctrl Pts',(43.930699644568,-4.11663984716378,337.69118179082));
#64316=CARTESIAN_POINT('Ctrl Pts',(43.9230064624217,-4.04235847274442,337.804808327266));
#64317=CARTESIAN_POINT('Ctrl Pts',(43.9153132802754,-3.9634556925758,337.915224547863));
#64318=CARTESIAN_POINT('Ctrl Pts',(43.9076200981291,-3.88026076241978,338.022045578433));
#64319=CARTESIAN_POINT('Ctrl Pts',(43.9006651991989,-3.80504970934187,338.118615431727));
#64320=CARTESIAN_POINT('Ctrl Pts',(43.8937103002687,-3.72633143770651,338.212247304725));
#64321=CARTESIAN_POINT('Ctrl Pts',(43.8867554013385,-3.64437438191438,338.302683519041));
#64322=CARTESIAN_POINT('Ctrl Pts',(43.87898032256,-3.5527522646666,338.4037847281));
#64323=CARTESIAN_POINT('Ctrl Pts',(43.8712052437816,-3.45677509712101,338.501230175163));
#64324=CARTESIAN_POINT('Ctrl Pts',(43.8634301650032,-3.35676612079108,338.594621575745));
#64325=CARTESIAN_POINT('Ctrl Pts',(43.8556646539542,-3.2568802118734,338.687898052262));
#64326=CARTESIAN_POINT('Ctrl Pts',(43.8478991429051,-3.15297264887849,338.777130144279));
#64327=CARTESIAN_POINT('Ctrl Pts',(43.8401336318561,-3.04540602346491,338.861953549014));
#64328=CARTESIAN_POINT('Ctrl Pts',(43.8323758203339,-2.93794605067338,338.946692851097));
#64329=CARTESIAN_POINT('Ctrl Pts',(43.8246180088117,-2.82683454027944,339.027031924415));
#64330=CARTESIAN_POINT('Ctrl Pts',(43.8168601972895,-2.71246966783161,339.102644435433));
#64331=CARTESIAN_POINT('Ctrl Pts',(43.8091082237665,-2.59819085857779,339.178200045639));
#64332=CARTESIAN_POINT('Ctrl Pts',(43.8013562502436,-2.48066388514998,339.249035958655));
#64333=CARTESIAN_POINT('Ctrl Pts',(43.7936042767206,-2.36031833378726,339.314867370579));
#64334=CARTESIAN_POINT('Ctrl Pts',(43.785855586163,-2.24002374883649,339.380670902862));
#64335=CARTESIAN_POINT('Ctrl Pts',(43.7781068956054,-2.1169133022824,339.441473962214));
#64336=CARTESIAN_POINT('Ctrl Pts',(43.7703582050478,-1.99144358419451,339.49703630333));
#64337=CARTESIAN_POINT('Ctrl Pts',(43.7626111266699,-1.86599997112941,339.552587084237));
#64338=CARTESIAN_POINT('Ctrl Pts',(43.7548640482921,-1.73819842007227,339.602899157572));
#64339=CARTESIAN_POINT('Ctrl Pts',(43.7471169699143,-1.60851766738135,339.647779467253));
#64340=CARTESIAN_POINT('Ctrl Pts',(43.7393698266085,-1.47883582784099,339.692660153075));
#64341=CARTESIAN_POINT('Ctrl Pts',(43.7316226833027,-1.34727512463209,339.732108856609));
#64342=CARTESIAN_POINT('Ctrl Pts',(43.7238755399969,-1.21433132587712,339.765981797436));
#64343=CARTESIAN_POINT('Ctrl Pts',(43.7161266549688,-1.08135763853389,339.79986235362));
#64344=CARTESIAN_POINT('Ctrl Pts',(43.7083777699407,-0.947000615589204,
339.828164556184));
#64345=CARTESIAN_POINT('Ctrl Pts',(43.7006288849126,-0.811767745687939,
339.850795418234));
#64346=CARTESIAN_POINT('Ctrl Pts',(43.6928717751379,-0.676391338220975,
339.873450300915));
#64347=CARTESIAN_POINT('Ctrl Pts',(43.6851146653632,-0.540137612890575,
339.89042175371));
#64348=CARTESIAN_POINT('Ctrl Pts',(43.6773575555884,-0.40352129152778,339.901668453678));
#64349=CARTESIAN_POINT('Ctrl Pts',(43.6695963006623,-0.266831966770898,
339.912921163523));
#64350=CARTESIAN_POINT('Ctrl Pts',(43.6618350457361,-0.129780050257217,
339.91844300923));
#64351=CARTESIAN_POINT('Ctrl Pts',(43.6540737908099,0.00711916348447759,
339.918244847505));
#64352=CARTESIAN_POINT('Ctrl Pts',(43.6463001204053,0.144237371352623,339.918046368786));
#64353=CARTESIAN_POINT('Ctrl Pts',(43.6385264500007,0.281201997602636,339.912109614865));
#64354=CARTESIAN_POINT('Ctrl Pts',(43.630752779596,0.41750140309195,339.900497489125));
#64355=CARTESIAN_POINT('Ctrl Pts',(43.6233409754188,0.547456038465653,339.889425910631));
#64356=CARTESIAN_POINT('Ctrl Pts',(43.6159291712417,0.676805705832155,339.873195482469));
#64357=CARTESIAN_POINT('Ctrl Pts',(43.6085173670645,0.80511693861203,339.851903727163));
#64358=CARTESIAN_POINT('Ctrl Pts',(43.600742288286,0.939717087128626,339.829568399505));
#64359=CARTESIAN_POINT('Ctrl Pts',(43.5929672095076,1.07359979499925,339.801592474557));
#64360=CARTESIAN_POINT('Ctrl Pts',(43.5851921307291,1.20625521177272,339.768032238416));
#64361=CARTESIAN_POINT('Ctrl Pts',(43.5774266196801,1.33874738761023,339.734513300281));
#64362=CARTESIAN_POINT('Ctrl Pts',(43.5696611086311,1.47001490202124,339.695423818914));
#64363=CARTESIAN_POINT('Ctrl Pts',(43.5618955975821,1.59955518587435,339.650871560239));
#64364=CARTESIAN_POINT('Ctrl Pts',(43.5541377860599,1.72896703015913,339.606363475258));
#64365=CARTESIAN_POINT('Ctrl Pts',(43.5463799745377,1.856654684722,339.556403518135));
#64366=CARTESIAN_POINT('Ctrl Pts',(43.5386221630155,1.98212825309632,339.501149925383));
#64367=CARTESIAN_POINT('Ctrl Pts',(43.5308701894925,2.10750739863111,339.445937912712));
#64368=CARTESIAN_POINT('Ctrl Pts',(43.5231182159695,2.23067541812224,339.385440350525));
#64369=CARTESIAN_POINT('Ctrl Pts',(43.5153662424465,2.35116034013002,339.319864363322));
#64370=CARTESIAN_POINT('Ctrl Pts',(43.5076175518889,2.47159423670197,339.254316147588));
#64371=CARTESIAN_POINT('Ctrl Pts',(43.4998688613313,2.5893469531945,339.183693970929));
#64372=CARTESIAN_POINT('Ctrl Pts',(43.4921201707736,2.70396937511788,339.108251779154));
#64373=CARTESIAN_POINT('Ctrl Pts',(43.4843730923958,2.81856794888919,339.032825283757));
#64374=CARTESIAN_POINT('Ctrl Pts',(43.476626014018,2.93003719724586,338.952580982734));
#64375=CARTESIAN_POINT('Ctrl Pts',(43.4688789356402,3.03795570349791,338.867816981979));
#64376=CARTESIAN_POINT('Ctrl Pts',(43.4611317923344,3.14587511421085,338.78305227082));
#64377=CARTESIAN_POINT('Ctrl Pts',(43.4533846490285,3.25024341607144,338.693768025815));
#64378=CARTESIAN_POINT('Ctrl Pts',(43.4456375057227,3.35067141248078,338.600303341121));
#64379=CARTESIAN_POINT('Ctrl Pts',(43.4378886206946,3.45112198723546,338.506817643581));
#64380=CARTESIAN_POINT('Ctrl Pts',(43.4301397356665,3.54763020769234,338.409149902393));
#64381=CARTESIAN_POINT('Ctrl Pts',(43.4223908506385,3.63984324796233,338.30767655504));
#64382=CARTESIAN_POINT('Ctrl Pts',(43.4146337408637,3.73215416410649,338.206095502827));
#64383=CARTESIAN_POINT('Ctrl Pts',(43.406876631089,3.82016052984577,338.10070106528));
#64384=CARTESIAN_POINT('Ctrl Pts',(43.3991195213143,3.90354905031887,337.991903720753));
#64385=CARTESIAN_POINT('Ctrl Pts',(43.3913582663881,3.98698213095089,337.883048238403));
#64386=CARTESIAN_POINT('Ctrl Pts',(43.383597011462,4.06579222487243,337.770786545488));
#64387=CARTESIAN_POINT('Ctrl Pts',(43.3758357565358,4.13970960628091,337.655557839356));
#64388=CARTESIAN_POINT('Ctrl Pts',(43.3680620861311,4.21374523141002,337.540144804847));
#64389=CARTESIAN_POINT('Ctrl Pts',(43.3602884157265,4.28287230667495,337.421755610424));
#64390=CARTESIAN_POINT('Ctrl Pts',(43.3525147453218,4.34686685157477,337.300854544985));
#64391=CARTESIAN_POINT('Ctrl Pts',(43.3451029411448,4.40788243501296,337.185581453231));
#64392=CARTESIAN_POINT('Ctrl Pts',(43.3376911369677,4.46423244880345,337.06802534241));
#64393=CARTESIAN_POINT('Ctrl Pts',(43.3302793327907,4.51576432808058,336.948603498851));
#64394=CARTESIAN_POINT('Ctrl Pts',(43.3225042540122,4.56982193826697,336.823328434999));
#64395=CARTESIAN_POINT('Ctrl Pts',(43.3147291752338,4.61874800155502,336.695604231441));
#64396=CARTESIAN_POINT('Ctrl Pts',(43.3069540964554,4.66231394078948,336.565890091935));
#64397=CARTESIAN_POINT('Ctrl Pts',(43.2991885854064,4.70582626936205,336.436335573936));
#64398=CARTESIAN_POINT('Ctrl Pts',(43.2914230743574,4.74399147471954,336.304796359277));
#64399=CARTESIAN_POINT('Ctrl Pts',(43.2836575633084,4.77662821053168,336.171753387387));
#64400=CARTESIAN_POINT('Ctrl Pts',(43.2758997517862,4.80923258692527,336.038842327991));
#64401=CARTESIAN_POINT('Ctrl Pts',(43.268141940264,4.83631930973145,335.904430855672));
#64402=CARTESIAN_POINT('Ctrl Pts',(43.2603841287418,4.85775633232206,335.769016565677));
#64403=CARTESIAN_POINT('Ctrl Pts',(43.2526321552188,4.87917722287348,335.633704179228));
#64404=CARTESIAN_POINT('Ctrl Pts',(43.2448801816957,4.89495681489762,335.497390861714));
#64405=CARTESIAN_POINT('Ctrl Pts',(43.2371282081727,4.90501387297808,335.360585590939));
#64406=CARTESIAN_POINT('Ctrl Pts',(43.2293795176151,4.91506667188842,335.223838257278));
#64407=CARTESIAN_POINT('Ctrl Pts',(43.2216308270574,4.91940172842132,335.086599773745));
#64408=CARTESIAN_POINT('Ctrl Pts',(43.2138821364998,4.91798954940518,334.949385234946));
#64409=CARTESIAN_POINT('Ctrl Pts',(43.206135058122,4.91657766420467,334.812199244778));
#64410=CARTESIAN_POINT('Ctrl Pts',(43.1983879797441,4.90942092592708,334.675037580042));
#64411=CARTESIAN_POINT('Ctrl Pts',(43.1906409013663,4.89654196542704,334.538415941229));
#64412=CARTESIAN_POINT('Ctrl Pts',(43.1828937580605,4.8836628969889,334.401793157394));
#64413=CARTESIAN_POINT('Ctrl Pts',(43.1751466147547,4.86506154735705,334.265710797658));
#64414=CARTESIAN_POINT('Ctrl Pts',(43.1673994714489,4.84081245143042,334.13067964905));
#64415=CARTESIAN_POINT('Ctrl Pts',(43.1596505864208,4.81655790379226,333.995618142573));
#64416=CARTESIAN_POINT('Ctrl Pts',(43.1519017013927,4.78665315230708,333.861608702147));
#64417=CARTESIAN_POINT('Ctrl Pts',(43.1441528163646,4.75122381695227,333.729151738513));
#64418=CARTESIAN_POINT('Ctrl Pts',(43.1363957065899,4.71575687653477,333.596554183688));
#64419=CARTESIAN_POINT('Ctrl Pts',(43.1286385968151,4.67475373981558,333.465512775516));
#64420=CARTESIAN_POINT('Ctrl Pts',(43.1208814870404,4.62839004497313,333.336513103721));
#64421=CARTESIAN_POINT('Ctrl Pts',(43.1131202321142,4.58200157485461,333.207444498625));
#64422=CARTESIAN_POINT('Ctrl Pts',(43.1053589771881,4.53024698622739,333.080420165695));
#64423=CARTESIAN_POINT('Ctrl Pts',(43.0975977222619,4.47334964540293,332.955904598001));
#64424=CARTESIAN_POINT('Ctrl Pts',(43.0898240518573,4.41636128737603,332.831189845978));
#64425=CARTESIAN_POINT('Ctrl Pts',(43.0820503814527,4.3542139149992,332.708992227353));
#64426=CARTESIAN_POINT('Ctrl Pts',(43.074276711048,4.2871767500129,332.589751345473));
#64427=CARTESIAN_POINT('Ctrl Pts',(43.0668649068709,4.22326018118429,332.476061155331));
#64428=CARTESIAN_POINT('Ctrl Pts',(43.0594531026937,4.15489896546934,332.365058869625));
#64429=CARTESIAN_POINT('Ctrl Pts',(43.0520412985165,4.08236144624151,332.257098600981));
#64430=CARTESIAN_POINT('Ctrl Pts',(43.0442662197381,4.00626864711869,332.143846877975));
#64431=CARTESIAN_POINT('Ctrl Pts',(43.0364911409596,3.92533933969223,332.033585012205));
#64432=CARTESIAN_POINT('Ctrl Pts',(43.0287160621812,3.8398359819844,331.926753720582));
#64433=CARTESIAN_POINT('Ctrl Pts',(43.0209505511322,3.75443784160177,331.820053891664));
#64434=CARTESIAN_POINT('Ctrl Pts',(43.0131850400832,3.66447709226651,331.716776539489));
#64435=CARTESIAN_POINT('Ctrl Pts',(43.0054195290342,3.57026002930011,331.617334425977));
#64436=CARTESIAN_POINT('Ctrl Pts',(42.9976617175119,3.47613638282589,331.517990909609));
#64437=CARTESIAN_POINT('Ctrl Pts',(42.9899039059897,3.37776508815547,331.422475346331));
#64438=CARTESIAN_POINT('Ctrl Pts',(42.9821460944675,3.2754931257408,331.331168054309));
#64439=CARTESIAN_POINT('Ctrl Pts',(42.9743941209445,3.17329812622122,331.23992947392));
#64440=CARTESIAN_POINT('Ctrl Pts',(42.9666421474215,3.06720859208385,331.152893120581));
#64441=CARTESIAN_POINT('Ctrl Pts',(42.9588901738985,2.95760857247817,331.070402743982));
#64442=CARTESIAN_POINT('Ctrl Pts',(42.9511414833409,2.84805496854586,330.987947302107));
#64443=CARTESIAN_POINT('Ctrl Pts',(42.9433927927833,2.73499414772412,330.910034242402));
#64444=CARTESIAN_POINT('Ctrl Pts',(42.9356441022256,2.61884330360773,330.836967113552));
#64445=CARTESIAN_POINT('Ctrl Pts',(42.9278970238478,2.50271662564458,330.763915186928));
#64446=CARTESIAN_POINT('Ctrl Pts',(42.9201499454699,2.38350153381684,330.695707393705));
#64447=CARTESIAN_POINT('Ctrl Pts',(42.9124028670921,2.26164393852248,330.63260377824));
#64448=CARTESIAN_POINT('Ctrl Pts',(42.9046557237863,2.13978532194394,330.569499633906));
#64449=CARTESIAN_POINT('Ctrl Pts',(42.8969085804805,2.01528450482106,330.511499932397));
#64450=CARTESIAN_POINT('Ctrl Pts',(42.8891614371747,1.88861135397397,330.458818411895));
#64451=CARTESIAN_POINT('Ctrl Pts',(42.8814125521465,1.76190972431323,330.40612504747));
#64452=CARTESIAN_POINT('Ctrl Pts',(42.8736636671184,1.63303514992976,330.358752393309));
#64453=CARTESIAN_POINT('Ctrl Pts',(42.8659147820903,1.50247641706839,330.316865613859));
#64454=CARTESIAN_POINT('Ctrl Pts',(42.8581576723156,1.3717791078192,330.274934375349));
#64455=CARTESIAN_POINT('Ctrl Pts',(42.8504005625409,1.23939444200347,330.238500762664));
#64456=CARTESIAN_POINT('Ctrl Pts',(42.8426434527661,1.1058258102754,330.207679858375));
#64457=CARTESIAN_POINT('Ctrl Pts',(42.83488219784,0.972185803741678,330.17684248438));
#64458=CARTESIAN_POINT('Ctrl Pts',(42.8271209429138,0.837360954652679,330.15162386689));
#64459=CARTESIAN_POINT('Ctrl Pts',(42.8193596879877,0.701862741466809,330.132087536259));
#64460=CARTESIAN_POINT('Ctrl Pts',(42.811586017583,0.566147775298238,330.112519953867));
#64461=CARTESIAN_POINT('Ctrl Pts',(42.8038123471784,0.429757681615977,330.098652862019));
#64462=CARTESIAN_POINT('Ctrl Pts',(42.7960386767737,0.293207823584374,330.090497761006));
#64463=CARTESIAN_POINT('Ctrl Pts',(42.7886268725967,0.163014394297436,330.082722281907));
#64464=CARTESIAN_POINT('Ctrl Pts',(42.7812150684197,0.0326760277303745,
330.080138980519));
#64465=CARTESIAN_POINT('Ctrl Pts',(42.7738032642427,-0.0973642792573438,
330.082713831835));
#64466=CARTESIAN_POINT('Ctrl Pts',(42.7660281854642,-0.233778249062257,
330.085414884285));
#64467=CARTESIAN_POINT('Ctrl Pts',(42.7582531066858,-0.370295296292574,
330.093801043059));
#64468=CARTESIAN_POINT('Ctrl Pts',(42.7504780279073,-0.506402781601683,
330.107890098814));
#64469=CARTESIAN_POINT('Ctrl Pts',(42.7427125168583,-0.642342777984723,
330.121961817088));
#64470=CARTESIAN_POINT('Ctrl Pts',(42.7349470058093,-0.777873830166071,
330.141722429118));
#64471=CARTESIAN_POINT('Ctrl Pts',(42.7271814947603,-0.91248308386811,330.16713773379));
#64472=CARTESIAN_POINT('Ctrl Pts',(42.7194236832382,-1.04695887210274,330.192527839114));
#64473=CARTESIAN_POINT('Ctrl Pts',(42.7116658717159,-1.18051429908788,330.22356140749));
#64474=CARTESIAN_POINT('Ctrl Pts',(42.7039080601938,-1.31264177613079,330.260152467636));
#64475=CARTESIAN_POINT('Ctrl Pts',(42.6961560866708,-1.44466982305722,330.296715991849));
#64476=CARTESIAN_POINT('Ctrl Pts',(42.6884041131478,-1.57527168375651,330.33882857949));
#64477=CARTESIAN_POINT('Ctrl Pts',(42.6806521396248,-1.70395046074921,330.386353298115));
#64478=CARTESIAN_POINT('Ctrl Pts',(42.6729034490672,-1.83257474220416,330.433857889995));
#64479=CARTESIAN_POINT('Ctrl Pts',(42.6651547585096,-1.95927719388752,330.486769919014));
#64480=CARTESIAN_POINT('Ctrl Pts',(42.6574060679519,-2.08357678784231,330.544902825789));
#64481=CARTESIAN_POINT('Ctrl Pts',(42.6496589895741,-2.20785052022823,330.603023637527));
#64482=CARTESIAN_POINT('Ctrl Pts',(42.6419119111963,-2.32972203544762,330.666363000912));
#64483=CARTESIAN_POINT('Ctrl Pts',(42.6341648328185,-2.44873134894977,330.7346866653));
#64484=CARTESIAN_POINT('Ctrl Pts',(42.6264176895126,-2.56774165986492,330.803010902306));
#64485=CARTESIAN_POINT('Ctrl Pts',(42.6186705462068,-2.6838893822343,330.876319329024));
#64486=CARTESIAN_POINT('Ctrl Pts',(42.6109234029009,-2.79674050716217,330.954332490417));
#64487=CARTESIAN_POINT('Ctrl Pts',(42.6031745178728,-2.90961700341836,331.032363190824));
#64488=CARTESIAN_POINT('Ctrl Pts',(42.5954256328448,-3.01919510597351,331.115100508432));
#64489=CARTESIAN_POINT('Ctrl Pts',(42.5876767478167,-3.1250714142378,331.20222279242));
#64490=CARTESIAN_POINT('Ctrl Pts',(42.5799196380419,-3.23106010070959,331.2894375489));
#64491=CARTESIAN_POINT('Ctrl Pts',(42.5721625282672,-3.33333884179704,331.381046320303));
#64492=CARTESIAN_POINT('Ctrl Pts',(42.5644054184925,-3.43153844854347,331.476688072471));
#64493=CARTESIAN_POINT('Ctrl Pts',(42.5566441635664,-3.52979053002,331.572380932533));
#64494=CARTESIAN_POINT('Ctrl Pts',(42.5488829086402,-3.62395886557364,331.672110783526));
#64495=CARTESIAN_POINT('Ctrl Pts',(42.541121653714,-3.71371324083096,331.775481892224));
#64496=CARTESIAN_POINT('Ctrl Pts',(42.5333479833094,-3.80361119383781,331.879018361007));
#64497=CARTESIAN_POINT('Ctrl Pts',(42.5255743129047,-3.88908083296764,331.986207421446));
#64498=CARTESIAN_POINT('Ctrl Pts',(42.5178006425,-3.96983359480141,332.096621917131));
#64499=CARTESIAN_POINT('Ctrl Pts',(42.510388838323,-4.04682729614372,332.201896591476));
#64500=CARTESIAN_POINT('Ctrl Pts',(42.5029770341459,-4.11953321835733,332.31010293196));
#64501=CARTESIAN_POINT('Ctrl Pts',(42.4955652299688,-4.18774024277605,332.420850000187));
#64502=CARTESIAN_POINT('Ctrl Pts',(42.4875585982108,-4.26142115969982,332.540484973317));
#64503=CARTESIAN_POINT('Ctrl Pts',(42.4795519664529,-4.33007336350018,332.663444420362));
#64504=CARTESIAN_POINT('Ctrl Pts',(42.471545334695,-4.39339327032408,332.789280968831));
#64505=CARTESIAN_POINT('Ctrl Pts',(42.4635504411677,-4.45662034614245,332.914933032927));
#64506=CARTESIAN_POINT('Ctrl Pts',(42.4555555476405,-4.51453053311371,333.043453480308));
#64507=CARTESIAN_POINT('Ctrl Pts',(42.4475606541133,-4.56686405814061,333.174367031147));
#64508=CARTESIAN_POINT('Ctrl Pts',(42.4395761882949,-4.61912932475261,333.305109831946));
#64509=CARTESIAN_POINT('Ctrl Pts',(42.4315917224765,-4.66583228396669,333.438239187889));
#64510=CARTESIAN_POINT('Ctrl Pts',(42.4236072566581,-4.70675956403405,333.573256340868));
#64511=CARTESIAN_POINT('Ctrl Pts',(42.4156345323191,-4.7476266588835,333.708074945672));
#64512=CARTESIAN_POINT('Ctrl Pts',(42.40766180798,-4.78273490269389,333.84477547108));
#64513=CARTESIAN_POINT('Ctrl Pts',(42.399689083641,-4.81191961162198,333.982840861129));
#64514=CARTESIAN_POINT('Ctrl Pts',(42.3917232936735,-4.84107893680364,334.12078616717));
#64515=CARTESIAN_POINT('Ctrl Pts',(42.3837575037059,-4.86432491301446,334.260093623737));
#64516=CARTESIAN_POINT('Ctrl Pts',(42.3757917137383,-4.8815429408814,334.400232062518));
#64517=CARTESIAN_POINT('Ctrl Pts',(42.367832966357,-4.89874574622204,334.540246604354));
#64518=CARTESIAN_POINT('Ctrl Pts',(42.3598742189758,-4.9099311821094,334.681090308325));
#64519=CARTESIAN_POINT('Ctrl Pts',(42.3519154715946,-4.91503595708922,334.82222316512));
#64520=CARTESIAN_POINT('Ctrl Pts',(42.3485494398993,-4.91719494437154,334.881913169898));
#64521=CARTESIAN_POINT('Ctrl Pts',(42.345183408204,-4.91826689118854,334.941654801808));
#64522=CARTESIAN_POINT('Ctrl Pts',(42.3418173765087,-4.91824979877537,335.001406892326));
#64523=CARTESIAN_POINT('',(40.5918173765378,-4.91824844260515,335.003913989273));
#64524=CARTESIAN_POINT('Ctrl Pts',(42.3418173764773,-4.91824979877521,335.001406892883));
#64525=CARTESIAN_POINT('Ctrl Pts',(42.3335008810188,-4.91820756832534,335.14903710983));
#64526=CARTESIAN_POINT('Ctrl Pts',(42.3251843855604,-4.91151404239866,335.296481149157));
#64527=CARTESIAN_POINT('Ctrl Pts',(42.3168678901019,-4.89824458647915,335.443151253555));
#64528=CARTESIAN_POINT('Ctrl Pts',(42.3085205834487,-4.88492596949262,335.590364745631));
#64529=CARTESIAN_POINT('Ctrl Pts',(42.3001732767955,-4.86498268740323,335.736798269062));
#64530=CARTESIAN_POINT('Ctrl Pts',(42.2918259701422,-4.83854181084379,335.881870856314));
#64531=CARTESIAN_POINT('Ctrl Pts',(42.2834633353011,-4.81205238081165,336.027209840859));
#64532=CARTESIAN_POINT('Ctrl Pts',(42.2751007004599,-4.77904159042933,336.171182611566));
#64533=CARTESIAN_POINT('Ctrl Pts',(42.2667380656187,-4.73968664218145,336.313222599724));
#64534=CARTESIAN_POINT('Ctrl Pts',(42.258349086423,-4.70020771617673,336.455710048746));
#64535=CARTESIAN_POINT('Ctrl Pts',(42.2499601072272,-4.65434472893535,336.596252249629));
#64536=CARTESIAN_POINT('Ctrl Pts',(42.2415711280315,-4.60232439377681,336.734299062142));
#64537=CARTESIAN_POINT('Ctrl Pts',(42.2334898172526,-4.55221192056292,336.867282964941));
#64538=CARTESIAN_POINT('Ctrl Pts',(42.2254085064738,-4.49638586911976,336.997951091023));
#64539=CARTESIAN_POINT('Ctrl Pts',(42.2173271956949,-4.4350887964449,337.125834055177));
#64540=CARTESIAN_POINT('Ctrl Pts',(42.2095521169165,-4.37611450601408,337.248871041122));
#64541=CARTESIAN_POINT('Ctrl Pts',(42.2017770381381,-4.31192325927031,337.369646517461));
#64542=CARTESIAN_POINT('Ctrl Pts',(42.1940019593596,-4.24271124933489,337.48768653919));
#64543=CARTESIAN_POINT('Ctrl Pts',(42.1862364483106,-4.17358440918395,337.605581305158));
#64544=CARTESIAN_POINT('Ctrl Pts',(42.1784709372616,-4.09944929484068,337.720746980229));
#64545=CARTESIAN_POINT('Ctrl Pts',(42.1707054262125,-4.02054950834209,337.832730963835));
#64546=CARTESIAN_POINT('Ctrl Pts',(42.1629476146903,-3.94172795121146,337.944603914996));
#64547=CARTESIAN_POINT('Ctrl Pts',(42.1551898031681,-3.85815134700235,338.053301135164));
#64548=CARTESIAN_POINT('Ctrl Pts',(42.1474319916459,-3.7701082344178,338.158396264447));
#64549=CARTESIAN_POINT('Ctrl Pts',(42.1396800181229,-3.6821313770676,338.263412306313));
#64550=CARTESIAN_POINT('Ctrl Pts',(42.1319280445999,-3.58969495162526,338.364831354363));
#64551=CARTESIAN_POINT('Ctrl Pts',(42.1241760710769,-3.49312944932227,338.462257892298));
#64552=CARTESIAN_POINT('Ctrl Pts',(42.1164273805192,-3.39660484256669,338.559643170036));
#64553=CARTESIAN_POINT('Ctrl Pts',(42.1086786899616,-3.29595491151265,338.653039023564));
#64554=CARTESIAN_POINT('Ctrl Pts',(42.1009299994039,-3.1915487402333,338.742084940406));
#64555=CARTESIAN_POINT('Ctrl Pts',(42.0931829210261,-3.0871642915299,338.831112330502));
#64556=CARTESIAN_POINT('Ctrl Pts',(42.0854358426483,-2.9790254543068,338.915791330614));
#64557=CARTESIAN_POINT('Ctrl Pts',(42.0776887642704,-2.86753600020716,338.995800339108));
#64558=CARTESIAN_POINT('Ctrl Pts',(42.0699416209646,-2.75604561171866,339.075810018155));
#64559=CARTESIAN_POINT('Ctrl Pts',(42.0621944776588,-2.64120486790648,339.151149399624));
#64560=CARTESIAN_POINT('Ctrl Pts',(42.0544473343529,-2.52344792116647,339.221539251465));
#64561=CARTESIAN_POINT('Ctrl Pts',(42.0466984493248,-2.40566450016495,339.29194492844));
#64562=CARTESIAN_POINT('Ctrl Pts',(42.0389495642967,-2.28496390705461,339.357398661011));
#64563=CARTESIAN_POINT('Ctrl Pts',(42.0312006792686,-2.16180601742788,339.417666556624));
#64564=CARTESIAN_POINT('Ctrl Pts',(42.0234435694939,-2.03851740674447,339.477998421204));
#64565=CARTESIAN_POINT('Ctrl Pts',(42.0156864597192,-1.912766641066,339.53313328139));
#64566=CARTESIAN_POINT('Ctrl Pts',(42.0079293499445,-1.78503526660596,339.58288469847));
#64567=CARTESIAN_POINT('Ctrl Pts',(42.0001680950183,-1.65723563658356,339.632662701117));
#64568=CARTESIAN_POINT('Ctrl Pts',(41.9924068400921,-1.52745365852669,339.677051402064));
#64569=CARTESIAN_POINT('Ctrl Pts',(41.9846455851659,-1.39618631264649,339.715914210721));
#64570=CARTESIAN_POINT('Ctrl Pts',(41.9768719147613,-1.2647089817928,339.754839187207));
#64571=CARTESIAN_POINT('Ctrl Pts',(41.9690982443566,-1.13174191426479,339.788220511985));
#64572=CARTESIAN_POINT('Ctrl Pts',(41.9613245739519,-0.997793433939985,
339.815972521276));
#64573=CARTESIAN_POINT('Ctrl Pts',(41.9539127697749,-0.870080287601892,
339.842432667857));
#64574=CARTESIAN_POINT('Ctrl Pts',(41.9465009655979,-0.741475325697093,
339.863775746802));
#64575=CARTESIAN_POINT('Ctrl Pts',(41.9390891614209,-0.612421823419636,
339.879971574989));
#64576=CARTESIAN_POINT('Ctrl Pts',(41.9313140826425,-0.477043024563564,
339.89696120896));
#64577=CARTESIAN_POINT('Ctrl Pts',(41.923539003864,-0.340742782972515,339.908339960455));
#64578=CARTESIAN_POINT('Ctrl Pts',(41.9157639250856,-0.204025820466614,
339.91401633362));
#64579=CARTESIAN_POINT('Ctrl Pts',(41.9079984140366,-0.0674770968869047,
339.919685721646));
#64580=CARTESIAN_POINT('Ctrl Pts',(41.9002329029876,0.0694869404750382,
339.919666677377));
#64581=CARTESIAN_POINT('Ctrl Pts',(41.8924673919386,0.206353863106128,339.913919122827));
#64582=CARTESIAN_POINT('Ctrl Pts',(41.8847095804164,0.343085081785045,339.908177266993));
#64583=CARTESIAN_POINT('Ctrl Pts',(41.8769517688942,0.479718989340334,339.896718220363));
#64584=CARTESIAN_POINT('Ctrl Pts',(41.869193957372,0.615740905792668,339.879553893486));
#64585=CARTESIAN_POINT('Ctrl Pts',(41.861441983849,0.751660461439184,339.862402483309));
#64586=CARTESIAN_POINT('Ctrl Pts',(41.853690010326,0.886968556433025,339.839554387434));
#64587=CARTESIAN_POINT('Ctrl Pts',(41.845938036803,1.02115374490959,339.811073486422));
#64588=CARTESIAN_POINT('Ctrl Pts',(41.8381893462454,1.15528210587917,339.78260464709));
#64589=CARTESIAN_POINT('Ctrl Pts',(41.8304406556877,1.28828812460929,339.748507828192));
#64590=CARTESIAN_POINT('Ctrl Pts',(41.8226919651301,1.41966890589686,339.708898306412));
#64591=CARTESIAN_POINT('Ctrl Pts',(41.8149448867523,1.55102235231557,339.669297025724));
#64592=CARTESIAN_POINT('Ctrl Pts',(41.8071978083745,1.68075085988325,339.624185436303));
#64593=CARTESIAN_POINT('Ctrl Pts',(41.7994507299967,1.8083654829202,339.57372904124));
#64594=CARTESIAN_POINT('Ctrl Pts',(41.7917035866909,1.9359811754906,339.523272223304));
#64595=CARTESIAN_POINT('Ctrl Pts',(41.7839564433851,2.06148258469986,339.467470654098));
#64596=CARTESIAN_POINT('Ctrl Pts',(41.7762093000793,2.18439995358816,339.406538313151));
#64597=CARTESIAN_POINT('Ctrl Pts',(41.7684604150512,2.3073449569106,339.345592273319));
#64598=CARTESIAN_POINT('Ctrl Pts',(41.7607115300231,2.42770441375425,339.279513339967));
#64599=CARTESIAN_POINT('Ctrl Pts',(41.752962644995,2.54503277380992,339.208561659609));
#64600=CARTESIAN_POINT('Ctrl Pts',(41.7452055352202,2.66248566739918,339.137534670405));
#64601=CARTESIAN_POINT('Ctrl Pts',(41.7374484254455,2.77690070246621,339.061624805255));
#64602=CARTESIAN_POINT('Ctrl Pts',(41.7296913156707,2.88786050643372,338.98113611396));
#64603=CARTESIAN_POINT('Ctrl Pts',(41.7219300607446,2.99887960377259,338.900604412083));
#64604=CARTESIAN_POINT('Ctrl Pts',(41.7141688058185,3.10643948460496,338.815489251063));
#64605=CARTESIAN_POINT('Ctrl Pts',(41.7064075508923,3.21015634248099,338.726134635159));
#64606=CARTESIAN_POINT('Ctrl Pts',(41.6986338804877,3.31403911352837,338.636637080989));
#64607=CARTESIAN_POINT('Ctrl Pts',(41.690860210083,3.41406629158227,338.542886787435));
#64608=CARTESIAN_POINT('Ctrl Pts',(41.6830865396784,3.50989075692392,338.445264857302));
#64609=CARTESIAN_POINT('Ctrl Pts',(41.6756747355012,3.60125457035065,338.352187251502));
#64610=CARTESIAN_POINT('Ctrl Pts',(41.6682629313241,3.68879794500973,338.255590560051));
#64611=CARTESIAN_POINT('Ctrl Pts',(41.6608511271469,3.77225561762683,338.155831208696));
#64612=CARTESIAN_POINT('Ctrl Pts',(41.6530760483685,3.85980379938591,338.051182354365));
#64613=CARTESIAN_POINT('Ctrl Pts',(41.6453009695901,3.94313231590458,337.94272226872));
#64614=CARTESIAN_POINT('Ctrl Pts',(41.6375258908116,4.02189109242853,337.830825869449));
#64615=CARTESIAN_POINT('Ctrl Pts',(41.6297603797626,4.10055295126395,337.719067165822));
#64616=CARTESIAN_POINT('Ctrl Pts',(41.6219948687136,4.17465603614357,337.603880878858));
#64617=CARTESIAN_POINT('Ctrl Pts',(41.6142293576646,4.24388934016124,337.485676232128));
#64618=CARTESIAN_POINT('Ctrl Pts',(41.6064715461424,4.31305399915637,337.367588785649));
#64619=CARTESIAN_POINT('Ctrl Pts',(41.5987137346202,4.37735828980762,337.246489270178));
#64620=CARTESIAN_POINT('Ctrl Pts',(41.590955923098,4.43653370507974,337.122816936571));
#64621=CARTESIAN_POINT('Ctrl Pts',(41.583203949575,4.49566458897523,336.999237670316));
#64622=CARTESIAN_POINT('Ctrl Pts',(41.575451976052,4.54967411188905,336.873089790863));
#64623=CARTESIAN_POINT('Ctrl Pts',(41.567700002529,4.59833921964451,336.744837953387));
#64624=CARTESIAN_POINT('Ctrl Pts',(41.5599513119714,4.64698371769801,336.61664043064));
#64625=CARTESIAN_POINT('Ctrl Pts',(41.5522026214138,4.69028816388154,336.48634108675));
#64626=CARTESIAN_POINT('Ctrl Pts',(41.5444539308562,4.72807735136723,336.35442519985));
#64627=CARTESIAN_POINT('Ctrl Pts',(41.5367068524783,4.76585867649684,336.222536759152));
#64628=CARTESIAN_POINT('Ctrl Pts',(41.5289597741005,4.79812691780422,336.089032819964));
#64629=CARTESIAN_POINT('Ctrl Pts',(41.5212126957227,4.82475665380657,335.954414110357));
#64630=CARTESIAN_POINT('Ctrl Pts',(41.5134655524169,4.85138661299176,335.819794272516));
#64631=CARTESIAN_POINT('Ctrl Pts',(41.505718409111,4.87237789676472,335.684060029066));
#64632=CARTESIAN_POINT('Ctrl Pts',(41.4979712658052,4.88765623263011,335.547722205257));
#64633=CARTESIAN_POINT('Ctrl Pts',(41.4902223807771,4.90293800338975,335.411353729811));
#64634=CARTESIAN_POINT('Ctrl Pts',(41.482473495749,4.91250422692397,335.27438179235));
#64635=CARTESIAN_POINT('Ctrl Pts',(41.4747246107209,4.91633255314925,335.13732184584));
#64636=CARTESIAN_POINT('Ctrl Pts',(41.4669675009462,4.92016494279956,335.000116422487));
#64637=CARTESIAN_POINT('Ctrl Pts',(41.4592103911715,4.91824725833746,334.862823194821));
#64638=CARTESIAN_POINT('Ctrl Pts',(41.4514532813968,4.91060931747564,334.725957679142));
#64639=CARTESIAN_POINT('Ctrl Pts',(41.4436920264706,4.90296729514245,334.589019026906));
#64640=CARTESIAN_POINT('Ctrl Pts',(41.4359307715444,4.88959896369185,334.45250893089));
#64641=CARTESIAN_POINT('Ctrl Pts',(41.4281695166183,4.87058590394933,334.316936302568));
#64642=CARTESIAN_POINT('Ctrl Pts',(41.4203958462136,4.85154242950756,334.181146802222));
#64643=CARTESIAN_POINT('Ctrl Pts',(41.412622175809,4.82683625318615,334.046298150978));
#64644=CARTESIAN_POINT('Ctrl Pts',(41.4048485054043,4.79660000606752,333.912888485806));
#64645=CARTESIAN_POINT('Ctrl Pts',(41.3974367012273,4.76777126352681,333.785689072645));
#64646=CARTESIAN_POINT('Ctrl Pts',(41.3900248970502,4.73391578815166,333.659797968779));
#64647=CARTESIAN_POINT('Ctrl Pts',(41.3826130928731,4.69518975677905,333.535631122177));
#64648=CARTESIAN_POINT('Ctrl Pts',(41.3748380140947,4.65456564724977,333.405378488548));
#64649=CARTESIAN_POINT('Ctrl Pts',(41.3670629353163,4.60845308901366,333.276611785491));
#64650=CARTESIAN_POINT('Ctrl Pts',(41.3592878565378,4.55697791281717,333.149828287808));
#64651=CARTESIAN_POINT('Ctrl Pts',(41.3515223454888,4.50556608010206,333.02320080529));
#64652=CARTESIAN_POINT('Ctrl Pts',(41.3437568344398,4.44880490526497,332.898552031031));
#64653=CARTESIAN_POINT('Ctrl Pts',(41.3359913233908,4.386870209454,332.776364951728));
#64654=CARTESIAN_POINT('Ctrl Pts',(41.3282335118686,4.32499692207421,332.654299021269));
#64655=CARTESIAN_POINT('Ctrl Pts',(41.3204757003464,4.25796049742053,332.534690274878));
#64656=CARTESIAN_POINT('Ctrl Pts',(41.3127178888242,4.18598500634489,332.418002209692));
#64657=CARTESIAN_POINT('Ctrl Pts',(41.3049659153011,4.11406367910875,332.301401955975));
#64658=CARTESIAN_POINT('Ctrl Pts',(41.2972139417781,4.03721088794364,332.187718339978));
#64659=CARTESIAN_POINT('Ctrl Pts',(41.2894619682551,3.95569666388645,332.077390384294));
#64660=CARTESIAN_POINT('Ctrl Pts',(41.2817132776974,3.87421696115165,331.967109152565));
#64661=CARTESIAN_POINT('Ctrl Pts',(41.2739645871398,3.78807998369841,331.860181068356));
#64662=CARTESIAN_POINT('Ctrl Pts',(41.2662158965822,3.69759899779396,331.757016078669));
#64663=CARTESIAN_POINT('Ctrl Pts',(41.2584688182044,3.60713683721434,331.653872553319));
#64664=CARTESIAN_POINT('Ctrl Pts',(41.2507217398265,3.51233272349198,331.554490858842));
#64665=CARTESIAN_POINT('Ctrl Pts',(41.2429746614487,3.41353985678451,331.459247437529));
#64666=CARTESIAN_POINT('Ctrl Pts',(41.2352275181429,3.31474616209768,331.364003217985));
#64667=CARTESIAN_POINT('Ctrl Pts',(41.2274803748371,3.21196392914661,331.272897612071));
#64668=CARTESIAN_POINT('Ctrl Pts',(41.2197332315313,3.10558252867318,331.186269513967));
#64669=CARTESIAN_POINT('Ctrl Pts',(41.2119843465032,2.99917721140252,331.099621940027));
#64670=CARTESIAN_POINT('Ctrl Pts',(41.2042354614751,2.88917141948723,331.017454123762));
#64671=CARTESIAN_POINT('Ctrl Pts',(41.196486576447,2.77598651341125,330.940063801011));
#64672=CARTESIAN_POINT('Ctrl Pts',(41.1887294666722,2.66268147170639,330.862591335372));
#64673=CARTESIAN_POINT('Ctrl Pts',(41.1809723568975,2.54619089844095,330.789906713775));
#64674=CARTESIAN_POINT('Ctrl Pts',(41.1732152471228,2.42696443834278,330.722263837318));
#64675=CARTESIAN_POINT('Ctrl Pts',(41.1654539921966,2.30767426743638,330.65458481467));
#64676=CARTESIAN_POINT('Ctrl Pts',(41.1576927372704,2.18564564415852,330.591953083886));
#64677=CARTESIAN_POINT('Ctrl Pts',(41.1499314823442,2.0613506710906,330.534575443108));
#64678=CARTESIAN_POINT('Ctrl Pts',(41.1421578119396,1.93685686657358,330.477106016804));
#64679=CARTESIAN_POINT('Ctrl Pts',(41.1343841415349,1.81008982922438,330.424907624753));
#64680=CARTESIAN_POINT('Ctrl Pts',(41.1266104711302,1.6815402273399,330.378138305148));
#64681=CARTESIAN_POINT('Ctrl Pts',(41.1191986669532,1.55897464035021,330.333546108623));
#64682=CARTESIAN_POINT('Ctrl Pts',(41.111786862776,1.4347889849869,330.293889000208));
#64683=CARTESIAN_POINT('Ctrl Pts',(41.1043750585989,1.30941755702012,330.259260740784));
#64684=CARTESIAN_POINT('Ctrl Pts',(41.0965999798205,1.17790130190658,330.222935247214));
#64685=CARTESIAN_POINT('Ctrl Pts',(41.0888249010421,1.04466448298867,330.192029229547));
#64686=CARTESIAN_POINT('Ctrl Pts',(41.0810498222637,0.910193363494851,330.166705977954));
#64687=CARTESIAN_POINT('Ctrl Pts',(41.0732843112146,0.775887719274416,330.141413888233));
#64688=CARTESIAN_POINT('Ctrl Pts',(41.0655188001656,0.640351177074994,330.121690967004));
#64689=CARTESIAN_POINT('Ctrl Pts',(41.0577532891166,0.504085037626447,330.107650734326));
#64690=CARTESIAN_POINT('Ctrl Pts',(41.0499954775944,0.367954006451984,330.09362442258));
#64691=CARTESIAN_POINT('Ctrl Pts',(41.0422376660722,0.23109520394211,330.08526962641));
#64692=CARTESIAN_POINT('Ctrl Pts',(41.03447985455,0.0940196523223843,330.082648744753));
#64693=CARTESIAN_POINT('Ctrl Pts',(41.026727881027,-0.0429527455978324,
330.080029835393));
#64694=CARTESIAN_POINT('Ctrl Pts',(41.018975907504,-0.180141178734972,330.083136259286));
#64695=CARTESIAN_POINT('Ctrl Pts',(41.0112239339809,-0.317030334335458,
330.091978521888));
#64696=CARTESIAN_POINT('Ctrl Pts',(41.0034752434233,-0.453861517297275,
330.100817039787));
#64697=CARTESIAN_POINT('Ctrl Pts',(40.9957265528657,-0.590393285558151,
330.115386539881));
#64698=CARTESIAN_POINT('Ctrl Pts',(40.9879778623081,-0.726111379585388,
330.13564543573));
#64699=CARTESIAN_POINT('Ctrl Pts',(40.9802307839303,-0.861801236329623,
330.155900116546));
#64700=CARTESIAN_POINT('Ctrl Pts',(40.9724837055525,-0.99667736922515,330.18184178093));
#64701=CARTESIAN_POINT('Ctrl Pts',(40.9647366271746,-1.13023208304531,330.213377129859));
#64702=CARTESIAN_POINT('Ctrl Pts',(40.9569894838688,-1.26378791618261,330.244912743085));
#64703=CARTESIAN_POINT('Ctrl Pts',(40.949242340563,-1.39602192774177,330.282042044537));
#64704=CARTESIAN_POINT('Ctrl Pts',(40.9414951972572,-1.52643842352645,330.32462099914));
#64705=CARTESIAN_POINT('Ctrl Pts',(40.9337463122291,-1.6568842397082,330.367209526396));
#64706=CARTESIAN_POINT('Ctrl Pts',(40.925997427201,-1.78551135551533,330.415250023519));
#64707=CARTESIAN_POINT('Ctrl Pts',(40.9182485421729,-1.91184137619329,330.468549281436));
#64708=CARTESIAN_POINT('Ctrl Pts',(40.9104914323981,-2.03830548486043,330.521905111736));
#64709=CARTESIAN_POINT('Ctrl Pts',(40.9027343226234,-2.16246726724153,330.580530700623));
#64710=CARTESIAN_POINT('Ctrl Pts',(40.8949772128487,-2.28386988392361,330.644185332707));
#64711=CARTESIAN_POINT('Ctrl Pts',(40.8872159579225,-2.40533737428225,330.70787397979));
#64712=CARTESIAN_POINT('Ctrl Pts',(40.8794547029963,-2.52404242294461,330.776596829136));
#64713=CARTESIAN_POINT('Ctrl Pts',(40.8716934480702,-2.63955564714407,330.850068789952));
#64714=CARTESIAN_POINT('Ctrl Pts',(40.8639197776655,-2.75525365485657,330.923658281961));
#64715=CARTESIAN_POINT('Ctrl Pts',(40.8561461072609,-2.86774931413656,331.002011843043));
#64716=CARTESIAN_POINT('Ctrl Pts',(40.8483724368562,-2.97664419852648,331.084802383292));
#64717=CARTESIAN_POINT('Ctrl Pts',(40.8409606326792,-3.08046999984856,331.163739003973));
#64718=CARTESIAN_POINT('Ctrl Pts',(40.8335488285022,-3.18102249224915,331.246708634064));
#64719=CARTESIAN_POINT('Ctrl Pts',(40.8261370243251,-3.277987807843,331.33339680438));
#64720=CARTESIAN_POINT('Ctrl Pts',(40.8184774883965,-3.37819408702793,331.422982435525));
#64721=CARTESIAN_POINT('Ctrl Pts',(40.8108179524678,-3.47490617038605,331.516841100302));
#64722=CARTESIAN_POINT('Ctrl Pts',(40.8031584165391,-3.56772938716284,331.614665440097));
#64723=CARTESIAN_POINT('Ctrl Pts',(40.7955083882634,-3.66043738404334,331.712368352185));
#64724=CARTESIAN_POINT('Ctrl Pts',(40.7878583599877,-3.74926583893483,331.814026860542));
#64725=CARTESIAN_POINT('Ctrl Pts',(40.780208331712,-3.83385327521381,331.919293566951));
#64726=CARTESIAN_POINT('Ctrl Pts',(40.7723587085798,-3.92064765983382,332.027306759047));
#64727=CARTESIAN_POINT('Ctrl Pts',(40.7645090854475,-4.00297633942959,332.139118761692));
#64728=CARTESIAN_POINT('Ctrl Pts',(40.7566594623152,-4.08048871165239,332.254313394326));
#64729=CARTESIAN_POINT('Ctrl Pts',(40.7490228558809,-4.15589761606571,332.366381968569));
#64730=CARTESIAN_POINT('Ctrl Pts',(40.7413862494465,-4.22674798672772,332.481651599997));
#64731=CARTESIAN_POINT('Ctrl Pts',(40.7337496430121,-4.2927580134138,332.599705913691));
#64732=CARTESIAN_POINT('Ctrl Pts',(40.7261160083527,-4.35874235238795,332.717714286709));
#64733=CARTESIAN_POINT('Ctrl Pts',(40.7184823736934,-4.41988989621217,332.838504835659));
#64734=CARTESIAN_POINT('Ctrl Pts',(40.710848739034,-4.47596320614106,332.961633879851));
#64735=CARTESIAN_POINT('Ctrl Pts',(40.7032163086797,-4.53202766977587,333.084743498835));
#64736=CARTESIAN_POINT('Ctrl Pts',(40.6955838783255,-4.58301932528335,333.210190511906));
#64737=CARTESIAN_POINT('Ctrl Pts',(40.6879514479713,-4.62874783466262,333.337508933676));
#64738=CARTESIAN_POINT('Ctrl Pts',(40.6799402753518,-4.67674551892118,333.471145247026));
#64739=CARTESIAN_POINT('Ctrl Pts',(40.6719291027324,-4.71894414040573,333.606843010139));
#64740=CARTESIAN_POINT('Ctrl Pts',(40.6639179301129,-4.75518202848812,333.744043416975));
#64741=CARTESIAN_POINT('Ctrl Pts',(40.6562793750924,-4.78973441115363,333.874862325298));
#64742=CARTESIAN_POINT('Ctrl Pts',(40.6486408200718,-4.81886799955878,334.007046828186));
#64743=CARTESIAN_POINT('Ctrl Pts',(40.6410022650512,-4.84249495174764,334.14010134039));
#64744=CARTESIAN_POINT('Ctrl Pts',(40.6333603033609,-4.86613244116799,334.273215192716));
#64745=CARTESIAN_POINT('Ctrl Pts',(40.6257183416706,-4.88425835008275,334.407199427809));
#64746=CARTESIAN_POINT('Ctrl Pts',(40.6180763799803,-4.89683667030984,334.541552961828));
#64747=CARTESIAN_POINT('Ctrl Pts',(40.6104262848455,-4.90942837781545,334.676049490153));
#64748=CARTESIAN_POINT('Ctrl Pts',(40.6027761897107,-4.91646069565557,334.810915700099));
#64749=CARTESIAN_POINT('Ctrl Pts',(40.5951260945759,-4.91794969000303,334.945650123284));
#64750=CARTESIAN_POINT('Ctrl Pts',(40.5940231885632,-4.91816435672152,334.965074640604));
#64751=CARTESIAN_POINT('Ctrl Pts',(40.5929202825506,-4.91826389528749,334.984496426894));
#64752=CARTESIAN_POINT('Ctrl Pts',(40.5918173765378,-4.91824844260515,335.003913989272));
#64753=CARTESIAN_POINT('',(38.8418173764735,-4.9182487714237,334.996523667274));
#64754=CARTESIAN_POINT('Ctrl Pts',(40.5918173765087,-4.91824844260474,335.003913989785));
#64755=CARTESIAN_POINT('Ctrl Pts',(40.5790493522362,-4.91806955134227,335.228705499584));
#64756=CARTESIAN_POINT('Ctrl Pts',(40.5662813279637,-4.90247682601608,335.452900204882));
#64757=CARTESIAN_POINT('Ctrl Pts',(40.5535133036912,-4.87172844847187,335.674866643753));
#64758=CARTESIAN_POINT('Ctrl Pts',(40.5516418658112,-4.86722158999028,335.707400761243));
#64759=CARTESIAN_POINT('Ctrl Pts',(40.5497704279312,-4.86238919688565,335.739887074424));
#64760=CARTESIAN_POINT('Ctrl Pts',(40.5478989900512,-4.85723214447028,335.772320501621));
#64761=CARTESIAN_POINT('Ctrl Pts',(40.5401239112727,-4.8358066463429,335.907068469592));
#64762=CARTESIAN_POINT('Ctrl Pts',(40.5323488324943,-4.80873583282199,336.041137119539));
#64763=CARTESIAN_POINT('Ctrl Pts',(40.5245737537158,-4.77607254431648,336.174016232395));
#64764=CARTESIAN_POINT('Ctrl Pts',(40.5168082426668,-4.74344945006692,336.306731829042));
#64765=CARTESIAN_POINT('Ctrl Pts',(40.5090427316178,-4.70524766624566,336.438260425195));
#64766=CARTESIAN_POINT('Ctrl Pts',(40.5012772205688,-4.66157156110468,336.568098735157));
#64767=CARTESIAN_POINT('Ctrl Pts',(40.4935194090466,-4.61793876094902,336.697808310056));
#64768=CARTESIAN_POINT('Ctrl Pts',(40.4857615975244,-4.5688425649342,336.825830565857));
#64769=CARTESIAN_POINT('Ctrl Pts',(40.4780037860021,-4.51443789636349,336.951674548273));
#64770=CARTESIAN_POINT('Ctrl Pts',(40.4702518124791,-4.46007416903115,337.077423829102));
#64771=CARTESIAN_POINT('Ctrl Pts',(40.462499838956,-4.40041007506831,337.200997741995));
#64772=CARTESIAN_POINT('Ctrl Pts',(40.454747865433,-4.33564954574583,337.32192292701));
#64773=CARTESIAN_POINT('Ctrl Pts',(40.4469991748753,-4.27091644254605,337.442796900137));
#64774=CARTESIAN_POINT('Ctrl Pts',(40.4392504843177,-4.20109138092865,337.561024032588));
#64775=CARTESIAN_POINT('Ctrl Pts',(40.4315017937601,-4.12642526682002,337.676153504538));
#64776=CARTESIAN_POINT('Ctrl Pts',(40.4237547153822,-4.05177468762015,337.791259022839));
#64777=CARTESIAN_POINT('Ctrl Pts',(40.4160076370044,-3.97228527191546,337.903267834844));
#64778=CARTESIAN_POINT('Ctrl Pts',(40.4082605586266,-3.8882522718278,338.011756519562));
#64779=CARTESIAN_POINT('Ctrl Pts',(40.4005134153208,-3.80421856746266,338.12024611352));
#64780=CARTESIAN_POINT('Ctrl Pts',(40.392766272015,-3.71564144211904,338.225215212332));
#64781=CARTESIAN_POINT('Ctrl Pts',(40.3850191287092,-3.62285735291542,338.326272337456));
#64782=CARTESIAN_POINT('Ctrl Pts',(40.3772702436811,-3.53005240387855,338.427352182368));
#64783=CARTESIAN_POINT('Ctrl Pts',(40.3695213586529,-3.43303887321729,338.52451801563));
#64784=CARTESIAN_POINT('Ctrl Pts',(40.3617724736248,-3.3321908062351,338.6174144763));
#64785=CARTESIAN_POINT('Ctrl Pts',(40.3540153638501,-3.2312356980728,338.710409538233));
#64786=CARTESIAN_POINT('Ctrl Pts',(40.3462582540754,-3.12643821129529,338.799125910124));
#64787=CARTESIAN_POINT('Ctrl Pts',(40.3385011443006,-3.01820669835919,338.883247531188));
#64788=CARTESIAN_POINT('Ctrl Pts',(40.3307398893745,-2.90991734996322,338.967414104157));
#64789=CARTESIAN_POINT('Ctrl Pts',(40.3229786344483,-2.79819063716515,339.04698080729));
#64790=CARTESIAN_POINT('Ctrl Pts',(40.3152173795221,-2.68346392510102,339.121674953848));
#64791=CARTESIAN_POINT('Ctrl Pts',(40.3074437091174,-2.56855368768694,339.196488586699));
#64792=CARTESIAN_POINT('Ctrl Pts',(40.2996700387128,-2.45063419752518,339.266413887778));
#64793=CARTESIAN_POINT('Ctrl Pts',(40.2918963683082,-2.33016821977328,339.331223745093));
#64794=CARTESIAN_POINT('Ctrl Pts',(40.2844845641312,-2.21530996227013,339.393016687957));
#64795=CARTESIAN_POINT('Ctrl Pts',(40.2770727599542,-2.09813721855394,339.450159591062));
#64796=CARTESIAN_POINT('Ctrl Pts',(40.2696609557773,-1.97906623474684,339.502497073956));
#64797=CARTESIAN_POINT('Ctrl Pts',(40.2618858769988,-1.85415922732714,339.557399772794));
#64798=CARTESIAN_POINT('Ctrl Pts',(40.2541107982204,-1.7267684688382,339.607187587518));
#64799=CARTESIAN_POINT('Ctrl Pts',(40.246335719442,-1.59735160835744,339.65162884394));
#64800=CARTESIAN_POINT('Ctrl Pts',(40.238570208393,-1.46809400356259,339.696015412568));
#64801=CARTESIAN_POINT('Ctrl Pts',(40.230804697344,-1.33681562377427,339.735068388041));
#64802=CARTESIAN_POINT('Ctrl Pts',(40.223039186295,-1.20399617232307,339.76860317908));
#64803=CARTESIAN_POINT('Ctrl Pts',(40.2152813747728,-1.07130841174459,339.802104720276));
#64804=CARTESIAN_POINT('Ctrl Pts',(40.2075235632506,-0.937082996803846,
339.830098870155));
#64805=CARTESIAN_POINT('Ctrl Pts',(40.1997657517284,-0.801816619324115,
339.852450223493));
#64806=CARTESIAN_POINT('Ctrl Pts',(40.1920137782054,-0.666652034083164,
339.874784756728));
#64807=CARTESIAN_POINT('Ctrl Pts',(40.1842618046824,-0.530448429629785,
339.891484882174));
#64808=CARTESIAN_POINT('Ctrl Pts',(40.1765098311594,-0.393714223350742,
339.902465927758));
#64809=CARTESIAN_POINT('Ctrl Pts',(40.1687611406018,-0.257037924089238,
339.913442322864));
#64810=CARTESIAN_POINT('Ctrl Pts',(40.1610124500441,-0.119831858743799,
339.918704424138));
#64811=CARTESIAN_POINT('Ctrl Pts',(40.1532637594865,0.0173890890826273,
339.918219259252));
#64812=CARTESIAN_POINT('Ctrl Pts',(40.1455166811087,0.154581486944766,339.917734195309));
#64813=CARTESIAN_POINT('Ctrl Pts',(40.1377696027309,0.291788370502441,339.911504245051));
#64814=CARTESIAN_POINT('Ctrl Pts',(40.1300225243531,0.428493898146529,339.899548554893));
#64815=CARTESIAN_POINT('Ctrl Pts',(40.1222753810473,0.56520057151461,339.887592764534));
#64816=CARTESIAN_POINT('Ctrl Pts',(40.1145282377414,0.701405491200203,339.869911172615));
#64817=CARTESIAN_POINT('Ctrl Pts',(40.1067810944356,0.836597378294582,339.846574861604));
#64818=CARTESIAN_POINT('Ctrl Pts',(40.0990322094075,0.971819659395384,339.823233304094));
#64819=CARTESIAN_POINT('Ctrl Pts',(40.0912833243795,1.10602806960277,339.794234564221));
#64820=CARTESIAN_POINT('Ctrl Pts',(40.0835344393514,1.23872136094388,339.759700878463));
#64821=CARTESIAN_POINT('Ctrl Pts',(40.0757773295767,1.37155549431541,339.725130538294));
#64822=CARTESIAN_POINT('Ctrl Pts',(40.0680202198019,1.50287091749337,339.685013615282));
#64823=CARTESIAN_POINT('Ctrl Pts',(40.0602631100272,1.63218086527492,339.639522463091));
#64824=CARTESIAN_POINT('Ctrl Pts',(40.052501855101,1.76155991215795,339.594007001884));
#64825=CARTESIAN_POINT('Ctrl Pts',(40.0447406001749,1.88893098547589,339.543111734109));
#64826=CARTESIAN_POINT('Ctrl Pts',(40.0369793452487,2.01382809376192,339.487056883));
#64827=CARTESIAN_POINT('Ctrl Pts',(40.0292056748441,2.13892499671734,339.430912362397));
#64828=CARTESIAN_POINT('Ctrl Pts',(40.0214320044394,2.2615396765308,339.369591940145));
#64829=CARTESIAN_POINT('Ctrl Pts',(40.0136583340347,2.38123072110303,339.303361862007));
#64830=CARTESIAN_POINT('Ctrl Pts',(40.0062465298576,2.49535011875538,339.24021480994));
#64831=CARTESIAN_POINT('Ctrl Pts',(39.9988347256805,2.60681170006456,339.172605053705));
#64832=CARTESIAN_POINT('Ctrl Pts',(39.9914229215033,2.71525954763402,339.100798538271));
#64833=CARTESIAN_POINT('Ctrl Pts',(39.9836478427249,2.8290227472616,339.025472571614));
#64834=CARTESIAN_POINT('Ctrl Pts',(39.9758727639464,2.93982883193801,338.945290008409));
#64835=CARTESIAN_POINT('Ctrl Pts',(39.968097685168,3.04723532172076,338.860510323333));
#64836=CARTESIAN_POINT('Ctrl Pts',(39.960332174119,3.15450964098001,338.775834965056));
#64837=CARTESIAN_POINT('Ctrl Pts',(39.95256666307,3.25839238526958,338.686573980678));
#64838=CARTESIAN_POINT('Ctrl Pts',(39.944801152021,3.35846873284634,338.593030870031));
#64839=CARTESIAN_POINT('Ctrl Pts',(39.9370433404988,3.45844585443319,338.49958050765));
#64840=CARTESIAN_POINT('Ctrl Pts',(39.9292855289766,3.5546238061729,338.401856733456));
#64841=CARTESIAN_POINT('Ctrl Pts',(39.9215277174544,3.64661993447727,338.300203950663));
#64842=CARTESIAN_POINT('Ctrl Pts',(39.9137757439313,3.73854683277773,338.198627664813));
#64843=CARTESIAN_POINT('Ctrl Pts',(39.9060237704083,3.82629791027722,338.093128544183));
#64844=CARTESIAN_POINT('Ctrl Pts',(39.8982717968853,3.90952683060465,337.984088306884));
#64845=CARTESIAN_POINT('Ctrl Pts',(39.8905231063277,3.9927205034348,337.875094248191));
#64846=CARTESIAN_POINT('Ctrl Pts',(39.8827744157701,4.07139559149932,337.762562365618));
#64847=CARTESIAN_POINT('Ctrl Pts',(39.8750257252125,4.14524573460145,337.646907792551));
#64848=CARTESIAN_POINT('Ctrl Pts',(39.8672786468346,4.21908051256449,337.531277282385));
#64849=CARTESIAN_POINT('Ctrl Pts',(39.8595315684567,4.2880921321048,337.412525703261));
#64850=CARTESIAN_POINT('Ctrl Pts',(39.8517844900789,4.35201754235686,337.291097198619));
#64851=CARTESIAN_POINT('Ctrl Pts',(39.8440373467731,4.41594348836542,337.169667676288));
#64852=CARTESIAN_POINT('Ctrl Pts',(39.8362902034673,4.47478295797907,337.045561529563));
#64853=CARTESIAN_POINT('Ctrl Pts',(39.8285430601615,4.52831904360689,336.919247170587));
#64854=CARTESIAN_POINT('Ctrl Pts',(39.8207941751334,4.58186716528338,336.792904413462));
#64855=CARTESIAN_POINT('Ctrl Pts',(39.8130452901053,4.6301093779028,336.664352816015));
#64856=CARTESIAN_POINT('Ctrl Pts',(39.8052964050772,4.67287721868922,336.534080037532));
#64857=CARTESIAN_POINT('Ctrl Pts',(39.7975392953025,4.71569045370373,336.403668986177));
#64858=CARTESIAN_POINT('Ctrl Pts',(39.7897821855277,4.7530175876444,336.271533476384));
#64859=CARTESIAN_POINT('Ctrl Pts',(39.782025075753,4.78474013980417,336.138176109856));
#64860=CARTESIAN_POINT('Ctrl Pts',(39.7742638208268,4.8164796434815,336.004747481415));
#64861=CARTESIAN_POINT('Ctrl Pts',(39.7665025659007,4.84260852332958,335.870096078756));
#64862=CARTESIAN_POINT('Ctrl Pts',(39.7587413109745,4.86305979504189,335.734732939473));
#64863=CARTESIAN_POINT('Ctrl Pts',(39.7509676405698,4.88354378212388,335.599153263282));
#64864=CARTESIAN_POINT('Ctrl Pts',(39.7431939701652,4.8983319697141,335.462859964112));
#64865=CARTESIAN_POINT('Ctrl Pts',(39.7354202997605,4.90740937613979,335.326368315673));
#64866=CARTESIAN_POINT('Ctrl Pts',(39.7280084955835,4.91606422711237,335.196230386308));
#64867=CARTESIAN_POINT('Ctrl Pts',(39.7205966914065,4.91952799801445,335.065912446114));
#64868=CARTESIAN_POINT('Ctrl Pts',(39.7131848872295,4.91783172031658,334.935857711703));
#64869=CARTESIAN_POINT('Ctrl Pts',(39.7054098084511,4.91605230299578,334.799428607344));
#64870=CARTESIAN_POINT('Ctrl Pts',(39.6976347296726,4.90858860544711,334.66285802097));
#64871=CARTESIAN_POINT('Ctrl Pts',(39.6898596508942,4.8954193741753,334.526658460043));
#64872=CARTESIAN_POINT('Ctrl Pts',(39.6820941398451,4.88226634848097,334.390626501346));
#64873=CARTESIAN_POINT('Ctrl Pts',(39.6743286287961,4.86342179614393,334.254965044991));
#64874=CARTESIAN_POINT('Ctrl Pts',(39.6665631177471,4.83891645279941,334.120187164604));
#64875=CARTESIAN_POINT('Ctrl Pts',(39.6588053062249,4.81443540657418,333.985542916879));
#64876=CARTESIAN_POINT('Ctrl Pts',(39.6510474947027,4.7843048083855,333.851780883789));
#64877=CARTESIAN_POINT('Ctrl Pts',(39.6432896831805,4.74860719843016,333.719409223242));
#64878=CARTESIAN_POINT('Ctrl Pts',(39.6355377096575,4.71293645205835,333.587137176567));
#64879=CARTESIAN_POINT('Ctrl Pts',(39.6277857361345,4.67170713398622,333.4562537957));
#64880=CARTESIAN_POINT('Ctrl Pts',(39.6200337626115,4.6250528166342,333.327256891856));
#64881=CARTESIAN_POINT('Ctrl Pts',(39.6122850720539,4.57841825741328,333.198314618277));
#64882=CARTESIAN_POINT('Ctrl Pts',(39.6045363814962,4.52636340112238,333.071257599526));
#64883=CARTESIAN_POINT('Ctrl Pts',(39.5967876909386,4.46907155320163,332.946568112923));
#64884=CARTESIAN_POINT('Ctrl Pts',(39.5890406125608,4.41179162532834,332.82190456901));
#64885=CARTESIAN_POINT('Ctrl Pts',(39.5812935341829,4.3492770362089,332.699607932412));
#64886=CARTESIAN_POINT('Ctrl Pts',(39.5735464558051,4.28175892361804,332.580139759714));
#64887=CARTESIAN_POINT('Ctrl Pts',(39.5657993124993,4.21424024516036,332.460670585757));
#64888=CARTESIAN_POINT('Ctrl Pts',(39.5580521691935,4.14171815190668,332.344030263272));
#64889=CARTESIAN_POINT('Ctrl Pts',(39.5503050258877,4.06446916047856,332.230654679167));
#64890=CARTESIAN_POINT('Ctrl Pts',(39.5425561408596,3.98720280183722,332.117253605824));
#64891=CARTESIAN_POINT('Ctrl Pts',(39.5348072558315,3.90520765040178,332.007119054362));
#64892=CARTESIAN_POINT('Ctrl Pts',(39.5270583708034,3.81880262439616,331.900656589146));
#64893=CARTESIAN_POINT('Ctrl Pts',(39.5193012610287,3.7323058872031,331.794081123569));
#64894=CARTESIAN_POINT('Ctrl Pts',(39.511544151254,3.64139017203667,331.691185834016));
#64895=CARTESIAN_POINT('Ctrl Pts',(39.5037870414792,3.54641401068168,331.592342340061));
#64896=CARTESIAN_POINT('Ctrl Pts',(39.4960257865531,3.45138709710289,331.493446027304));
#64897=CARTESIAN_POINT('Ctrl Pts',(39.4882645316268,3.35229569610611,331.39860609453));
#64898=CARTESIAN_POINT('Ctrl Pts',(39.4805032767007,3.24953330105455,331.308155422037));
#64899=CARTESIAN_POINT('Ctrl Pts',(39.472729606296,3.14660651966109,331.217560057945));
#64900=CARTESIAN_POINT('Ctrl Pts',(39.4649559358914,3.03999731354977,331.13136823082));
#64901=CARTESIAN_POINT('Ctrl Pts',(39.4571822654867,2.93013087993433,331.049871383239));
#64902=CARTESIAN_POINT('Ctrl Pts',(39.4497704613096,2.82537875523543,330.972168233519));
#64903=CARTESIAN_POINT('Ctrl Pts',(39.4423586571325,2.717666064299,330.898732959589));
#64904=CARTESIAN_POINT('Ctrl Pts',(39.4349468529553,2.60738231034018,330.829779316364));
#64905=CARTESIAN_POINT('Ctrl Pts',(39.4271717741769,2.49169322108207,330.757446049682));
#64906=CARTESIAN_POINT('Ctrl Pts',(39.4193966953984,2.37280906638468,330.689816251477));
#64907=CARTESIAN_POINT('Ctrl Pts',(39.41162161662,2.25114932321885,330.62718514146));
#64908=CARTESIAN_POINT('Ctrl Pts',(39.403856105571,2.12963929011222,330.56463110301));
#64909=CARTESIAN_POINT('Ctrl Pts',(39.396090594522,2.00536080868306,330.507063690815));
#64910=CARTESIAN_POINT('Ctrl Pts',(39.388325083473,1.87876196630618,330.454734712202));
#64911=CARTESIAN_POINT('Ctrl Pts',(39.3805672719508,1.75228864705019,330.402457617924));
#64912=CARTESIAN_POINT('Ctrl Pts',(39.3728094604286,1.62349990416403,330.35540876938));
#64913=CARTESIAN_POINT('Ctrl Pts',(39.3650516489064,1.49286772570919,330.31379375016));
#64914=CARTESIAN_POINT('Ctrl Pts',(39.3572996753834,1.36233385211122,330.272210047562));
#64915=CARTESIAN_POINT('Ctrl Pts',(39.3495477018604,1.22995967511856,330.236052153244));
#64916=CARTESIAN_POINT('Ctrl Pts',(39.3417957283374,1.09623609850447,330.205477137521));
#64917=CARTESIAN_POINT('Ctrl Pts',(39.3340470377797,0.962569153904467,330.174915070335));
#64918=CARTESIAN_POINT('Ctrl Pts',(39.3262983472222,0.827554326547805,330.149931266155));
#64919=CARTESIAN_POINT('Ctrl Pts',(39.3185496566645,0.691696370814679,330.130632567458));
#64920=CARTESIAN_POINT('Ctrl Pts',(39.3108025782867,0.555866681463951,330.111337884016));
#64921=CARTESIAN_POINT('Ctrl Pts',(39.3030554999089,0.419194599405768,330.097726008254));
#64922=CARTESIAN_POINT('Ctrl Pts',(39.295308421531,0.282193339330844,330.089852346239));
#64923=CARTESIAN_POINT('Ctrl Pts',(39.2875612782252,0.145190931053404,330.081978618234));
#64924=CARTESIAN_POINT('Ctrl Pts',(39.2798141349194,0.00785972948689445,
330.079843222325));
#64925=CARTESIAN_POINT('Ctrl Pts',(39.2720669916136,-0.129284079756904,
330.083449513203));
#64926=CARTESIAN_POINT('Ctrl Pts',(39.2643181065855,-0.26645872184048,330.087056614852));
#64927=CARTESIAN_POINT('Ctrl Pts',(39.2565692215574,-0.403445497104939,
330.096407961669));
#64928=CARTESIAN_POINT('Ctrl Pts',(39.2488203365293,-0.539730772873343,
330.111454842664));
#64929=CARTESIAN_POINT('Ctrl Pts',(39.2410632267546,-0.676160703241725,
330.126517694574));
#64930=CARTESIAN_POINT('Ctrl Pts',(39.2333061169799,-0.811887257620853,
330.147288113752));
#64931=CARTESIAN_POINT('Ctrl Pts',(39.2255490072052,-0.946403911061024,
330.173665707845));
#64932=CARTESIAN_POINT('Ctrl Pts',(39.217787752279,-1.08099244589969,330.200057397282));
#64933=CARTESIAN_POINT('Ctrl Pts',(39.2100264973528,-1.21436941163332,330.232062140864));
#64934=CARTESIAN_POINT('Ctrl Pts',(39.2022652424267,-1.34604194028045,330.269529182258));
#64935=CARTESIAN_POINT('Ctrl Pts',(39.194491572022,-1.47792510206144,330.307056158708));
#64936=CARTESIAN_POINT('Ctrl Pts',(39.1867179016173,-1.60809800697529,330.350062771191));
#64937=CARTESIAN_POINT('Ctrl Pts',(39.1789442312127,-1.73608547612891,330.398349178602));
#64938=CARTESIAN_POINT('Ctrl Pts',(39.1715324270356,-1.85811509780055,330.44438784213));
#64939=CARTESIAN_POINT('Ctrl Pts',(39.1641206228586,-1.97815790393833,330.495225701449));
#64940=CARTESIAN_POINT('Ctrl Pts',(39.1567088186816,-2.09582336093403,330.550650890044));
#64941=CARTESIAN_POINT('Ctrl Pts',(39.1489337399031,-2.2192559524852,330.608792632236));
#64942=CARTESIAN_POINT('Ctrl Pts',(39.1411586611247,-2.34046233029253,330.672166489798));
#64943=CARTESIAN_POINT('Ctrl Pts',(39.1333835823463,-2.45896723474375,330.74057947592));
#64944=CARTESIAN_POINT('Ctrl Pts',(39.1256180712973,-2.57732631136565,330.808908275507));
#64945=CARTESIAN_POINT('Ctrl Pts',(39.1178525602483,-2.69299019382656,330.882263671949));
#64946=CARTESIAN_POINT('Ctrl Pts',(39.1100870491993,-2.80550464618219,330.960405126408));
#64947=CARTESIAN_POINT('Ctrl Pts',(39.1023292376771,-2.91790754013065,331.038469103387));
#64948=CARTESIAN_POINT('Ctrl Pts',(39.0945714261548,-3.02716689928622,331.121309473258));
#64949=CARTESIAN_POINT('Ctrl Pts',(39.0868136146327,-3.13285442420018,331.208640584267));
#64950=CARTESIAN_POINT('Ctrl Pts',(39.0790616411097,-3.2384624159001,331.295905975845));
#64951=CARTESIAN_POINT('Ctrl Pts',(39.0713096675867,-3.34050362342662,331.387655134002));
#64952=CARTESIAN_POINT('Ctrl Pts',(39.0635576940637,-3.43858030680065,331.483560247042));
#64953=CARTESIAN_POINT('Ctrl Pts',(39.0558090035061,-3.53661545464118,331.57942474421));
#64954=CARTESIAN_POINT('Ctrl Pts',(39.0480603129484,-3.63068913881398,331.679441422937));
#64955=CARTESIAN_POINT('Ctrl Pts',(39.0403116223908,-3.72043836164334,331.783243643091));
#64956=CARTESIAN_POINT('Ctrl Pts',(39.032564544013,-3.81016891139729,331.887024266327));
#64957=CARTESIAN_POINT('Ctrl Pts',(39.0248174656351,-3.89557653396605,331.994588568876));
#64958=CARTESIAN_POINT('Ctrl Pts',(39.0170703872573,-3.97633690728958,332.10553496096));
#64959=CARTESIAN_POINT('Ctrl Pts',(39.0093232439515,-4.05709795746283,332.216482282881));
#64960=CARTESIAN_POINT('Ctrl Pts',(39.0015761006457,-4.13321145066981,332.330811434855));
#64961=CARTESIAN_POINT('Ctrl Pts',(38.9938289573398,-4.20439522822558,332.448090160806));
#64962=CARTESIAN_POINT('Ctrl Pts',(38.9860800723118,-4.27559500940562,332.565395253504));
#64963=CARTESIAN_POINT('Ctrl Pts',(38.9783311872837,-4.34186266676034,332.685650905652));
#64964=CARTESIAN_POINT('Ctrl Pts',(38.9705823022556,-4.40296120628621,332.80839883226));
#64965=CARTESIAN_POINT('Ctrl Pts',(38.9628251924808,-4.46412459643327,332.931277044786));
#64966=CARTESIAN_POINT('Ctrl Pts',(38.9550680827062,-4.520107734392,333.056652465586));
#64967=CARTESIAN_POINT('Ctrl Pts',(38.9473109729314,-4.57072093251787,333.184044818961));
#64968=CARTESIAN_POINT('Ctrl Pts',(38.9395497180053,-4.62136117671847,333.311505246736));
#64969=CARTESIAN_POINT('Ctrl Pts',(38.9317884630791,-4.666625634376,333.440984385878));
#64970=CARTESIAN_POINT('Ctrl Pts',(38.9240272081529,-4.7063743605626,333.571986190284));
#64971=CARTESIAN_POINT('Ctrl Pts',(38.9162535377483,-4.74618667175707,333.703197554884));
#64972=CARTESIAN_POINT('Ctrl Pts',(38.9084798673436,-4.78046552198303,333.835936073477));
#64973=CARTESIAN_POINT('Ctrl Pts',(38.9007061969389,-4.80912181532459,333.969694012504));
#64974=CARTESIAN_POINT('Ctrl Pts',(38.8932943927618,-4.83644415131691,334.097225487291));
#64975=CARTESIAN_POINT('Ctrl Pts',(38.8858825885847,-4.85865556129401,334.225683326727));
#64976=CARTESIAN_POINT('Ctrl Pts',(38.8784707844075,-4.87572286818258,334.354624469645));
#64977=CARTESIAN_POINT('Ctrl Pts',(38.8662529817746,-4.90385704200283,334.567174261542));
#64978=CARTESIAN_POINT('Ctrl Pts',(38.8540351791416,-4.91809686045341,334.781602982594));
#64979=CARTESIAN_POINT('Ctrl Pts',(38.8418173765087,-4.91824877142326,334.996523666654));
#64980=CARTESIAN_POINT('',(37.0918173765509,-4.91824956715858,334.997936593961));
#64981=CARTESIAN_POINT('Ctrl Pts',(38.8418173764734,-4.9182487714237,334.996523667274));
#64982=CARTESIAN_POINT('Ctrl Pts',(38.834160190451,-4.91834397760622,335.131219545687));
#64983=CARTESIAN_POINT('Ctrl Pts',(38.8265030044285,-4.91290165709758,335.266129879067));
#64984=CARTESIAN_POINT('Ctrl Pts',(38.8188458184061,-4.90189549404558,335.40075382463));
#64985=CARTESIAN_POINT('Ctrl Pts',(38.8111966330448,-4.89090083085527,335.535237107481));
#64986=CARTESIAN_POINT('Ctrl Pts',(38.8035474476834,-4.8743539196612,335.669434199112));
#64987=CARTESIAN_POINT('Ctrl Pts',(38.795898262322,-4.85228046796019,335.80284327409));
#64988=CARTESIAN_POINT('Ctrl Pts',(38.7882551171631,-4.8302244466272,335.936147002189));
#64989=CARTESIAN_POINT('Ctrl Pts',(38.7806119720041,-4.80265063162728,336.068663555743));
#64990=CARTESIAN_POINT('Ctrl Pts',(38.7729688268452,-4.76963658908505,336.199895774874));
#64991=CARTESIAN_POINT('Ctrl Pts',(38.7653291508184,-4.73663753122204,336.33106842927));
#64992=CARTESIAN_POINT('Ctrl Pts',(38.7576894747917,-4.69820325282644,336.460957518196));
#64993=CARTESIAN_POINT('Ctrl Pts',(38.7500497987649,-4.6544624227726,336.589076026343));
#64994=CARTESIAN_POINT('Ctrl Pts',(38.7424117446963,-4.61073087921174,336.717167334008));
#64995=CARTESIAN_POINT('Ctrl Pts',(38.7347736906278,-4.56169515389472,336.843488427036));
#64996=CARTESIAN_POINT('Ctrl Pts',(38.7271356365592,-4.50753363509457,336.967567938088));
#64997=CARTESIAN_POINT('Ctrl Pts',(38.7194974409813,-4.45337111285035,337.091649747946));
#64998=CARTESIAN_POINT('Ctrl Pts',(38.7118592454035,-4.39408276977663,337.213489523975));
#64999=CARTESIAN_POINT('Ctrl Pts',(38.7042210498256,-4.32989471712629,337.332636877249));
#65000=CARTESIAN_POINT('Ctrl Pts',(38.6965809493652,-4.26569065667752,337.45181394457));
#65001=CARTESIAN_POINT('Ctrl Pts',(38.6889408489049,-4.19658464836199,337.568296899509));
#65002=CARTESIAN_POINT('Ctrl Pts',(38.6813007484445,-4.12284794474613,337.681661404242));
#65003=CARTESIAN_POINT('Ctrl Pts',(38.6736526768816,-4.0490343098345,337.79514418492));
#65004=CARTESIAN_POINT('Ctrl Pts',(38.6660046053187,-3.97058055467107,337.905501682156));
#65005=CARTESIAN_POINT('Ctrl Pts',(38.6583565337558,-3.88780047989959,338.012339703784));
#65006=CARTESIAN_POINT('Ctrl Pts',(38.650704005967,-3.80497217248358,338.119239975661));
#65007=CARTESIAN_POINT('Ctrl Pts',(38.6430514781781,-3.71781278668029,338.22261638246));
#65008=CARTESIAN_POINT('Ctrl Pts',(38.6353989503893,-3.62667443205167,338.322110116538));
#65009=CARTESIAN_POINT('Ctrl Pts',(38.6277352273408,-3.53540274663827,338.421749404896));
#65010=CARTESIAN_POINT('Ctrl Pts',(38.6200715042925,-3.44014075536484,338.517494396713));
#65011=CARTESIAN_POINT('Ctrl Pts',(38.6124077812441,-3.34127548888804,338.609024961102));
#65012=CARTESIAN_POINT('Ctrl Pts',(38.6083494375406,-3.28892113981219,338.657495200346));
#65013=CARTESIAN_POINT('Ctrl Pts',(38.6042910938371,-3.23555687192711,338.704784305858));
#65014=CARTESIAN_POINT('Ctrl Pts',(38.6002327501337,-3.18124346485195,338.750849647725));
#65015=CARTESIAN_POINT('Ctrl Pts',(38.5924576713552,-3.07718844891677,338.839102809146));
#65016=CARTESIAN_POINT('Ctrl Pts',(38.5846825925768,-2.96929378179727,338.923162149202));
#65017=CARTESIAN_POINT('Ctrl Pts',(38.5769075137984,-2.85793200762272,339.002675068289));
#65018=CARTESIAN_POINT('Ctrl Pts',(38.5691420027494,-2.74670727120093,339.082090141668));
#65019=CARTESIAN_POINT('Ctrl Pts',(38.5613764917004,-2.63202423189635,339.156969700888));
#65020=CARTESIAN_POINT('Ctrl Pts',(38.5536109806514,-2.51429000286758,339.226999981545));
#65021=CARTESIAN_POINT('Ctrl Pts',(38.5458531691292,-2.39667250766975,339.296960826974));
#65022=CARTESIAN_POINT('Ctrl Pts',(38.538095357607,-2.27601017696682,339.362081763644));
#65023=CARTESIAN_POINT('Ctrl Pts',(38.5303375460848,-2.15274043763464,339.422091323195));
#65024=CARTESIAN_POINT('Ctrl Pts',(38.5225855725618,-2.02956346269024,339.482055723649));
#65025=CARTESIAN_POINT('Ctrl Pts',(38.5148335990388,-1.90378333472289,339.536916232802));
#65026=CARTESIAN_POINT('Ctrl Pts',(38.5070816255158,-1.77586319141563,339.586446662491));
#65027=CARTESIAN_POINT('Ctrl Pts',(38.4993329349581,-1.64799722236501,339.635956116014));
#65028=CARTESIAN_POINT('Ctrl Pts',(38.4915842444005,-1.51799340428276,339.680139838825));
#65029=CARTESIAN_POINT('Ctrl Pts',(38.4838355538429,-1.38633582058112,339.718819349697));
#65030=CARTESIAN_POINT('Ctrl Pts',(38.4760884754651,-1.2547056293394,339.757490812973));
#65031=CARTESIAN_POINT('Ctrl Pts',(38.4683413970872,-1.12142273166649,339.790660232078));
#65032=CARTESIAN_POINT('Ctrl Pts',(38.4605943187094,-0.986986996896747,
339.818198805618));
#65033=CARTESIAN_POINT('Ctrl Pts',(38.4528471754036,-0.852550135426429,
339.845737609957));
#65034=CARTESIAN_POINT('Ctrl Pts',(38.4451000320978,-0.71696080051072,339.867645396162));
#65035=CARTESIAN_POINT('Ctrl Pts',(38.437352888792,-0.580729303979137,339.883844442445));
#65036=CARTESIAN_POINT('Ctrl Pts',(38.4296040037639,-0.444467179714485,
339.900047130617));
#65037=CARTESIAN_POINT('Ctrl Pts',(38.4218551187358,-0.307562994614751,
339.910538478809));
#65038=CARTESIAN_POINT('Ctrl Pts',(38.4141062337077,-0.170532038893409,
339.915292655195));
#65039=CARTESIAN_POINT('Ctrl Pts',(38.406349123933,-0.0333556371000553,
339.920051877712));
#65040=CARTESIAN_POINT('Ctrl Pts',(38.3985920141582,0.103947412846171,339.919061750516));
#65041=CARTESIAN_POINT('Ctrl Pts',(38.3908349043835,0.24086140497208,339.912348607957));
#65042=CARTESIAN_POINT('Ctrl Pts',(38.3830736494573,0.377848559558,339.905631878109));
#65043=CARTESIAN_POINT('Ctrl Pts',(38.3753123945312,0.514445852999584,339.893186074617));
#65044=CARTESIAN_POINT('Ctrl Pts',(38.367551139605,0.650143834299697,339.875089338384));
#65045=CARTESIAN_POINT('Ctrl Pts',(38.3597774692003,0.786058888145837,339.85696365327));
#65046=CARTESIAN_POINT('Ctrl Pts',(38.3520037987957,0.921071369944786,339.833169039395));
#65047=CARTESIAN_POINT('Ctrl Pts',(38.344230128391,1.05468225807374,339.803834759544));
#65048=CARTESIAN_POINT('Ctrl Pts',(38.3368183242139,1.18207352721536,339.775865997478));
#65049=CARTESIAN_POINT('Ctrl Pts',(38.3294065200368,1.30819047607783,339.742861778726));
#65050=CARTESIAN_POINT('Ctrl Pts',(38.3219947158597,1.4326161110969,339.704975466538));
#65051=CARTESIAN_POINT('Ctrl Pts',(38.3142196370813,1.56314021713336,339.665232233332));
#65052=CARTESIAN_POINT('Ctrl Pts',(38.3064445583028,1.69221550488667,339.619990638147));
#65053=CARTESIAN_POINT('Ctrl Pts',(38.2986694795244,1.81934386082462,339.569373149413));
#65054=CARTESIAN_POINT('Ctrl Pts',(38.2909039684754,1.94631577722685,339.518817948722));
#65055=CARTESIAN_POINT('Ctrl Pts',(38.2831384574264,2.07134516913963,339.462900160397));
#65056=CARTESIAN_POINT('Ctrl Pts',(38.2753729463774,2.1939478730902,339.401792338657));
#65057=CARTESIAN_POINT('Ctrl Pts',(38.2676151348552,2.3164290161031,339.3407451055));
#65058=CARTESIAN_POINT('Ctrl Pts',(38.2598573233329,2.43648791178982,339.274518252865));
#65059=CARTESIAN_POINT('Ctrl Pts',(38.2520995118107,2.5536595598327,339.203332715236));
#65060=CARTESIAN_POINT('Ctrl Pts',(38.2443475382877,2.67074303249455,339.132200746982));
#65061=CARTESIAN_POINT('Ctrl Pts',(38.2365955647647,2.7849432495444,339.056117723371));
#65062=CARTESIAN_POINT('Ctrl Pts',(38.2288435912417,2.89581937415523,338.975350703368));
#65063=CARTESIAN_POINT('Ctrl Pts',(38.2210949006841,3.00664854266145,338.894617888245));
#65064=CARTESIAN_POINT('Ctrl Pts',(38.2133462101265,3.11415610337385,338.809205251785));
#65065=CARTESIAN_POINT('Ctrl Pts',(38.2055975195689,3.21793000230823,338.719423283621));
#65066=CARTESIAN_POINT('Ctrl Pts',(38.1978504411911,3.32168231021606,338.629659995346));
#65067=CARTESIAN_POINT('Ctrl Pts',(38.1901033628132,3.42170220608201,338.535529439166));
#65068=CARTESIAN_POINT('Ctrl Pts',(38.1823562844353,3.51761087008556,338.437382264043));
#65069=CARTESIAN_POINT('Ctrl Pts',(38.1746091411295,3.61352033789635,338.339234266352));
#65070=CARTESIAN_POINT('Ctrl Pts',(38.1668619978237,3.70531823193607,338.237069862133));
#65071=CARTESIAN_POINT('Ctrl Pts',(38.1591148545179,3.79266303528185,338.131276123772));
#65072=CARTESIAN_POINT('Ctrl Pts',(38.1513659694898,3.88002747559357,338.025458600733));
#65073=CARTESIAN_POINT('Ctrl Pts',(38.1436170844617,3.96293658422882,337.91601042126));
#65074=CARTESIAN_POINT('Ctrl Pts',(38.1358681994336,4.04108978555278,337.803350924804));
#65075=CARTESIAN_POINT('Ctrl Pts',(38.1281110896589,4.11932593949221,337.690571850394));
#65076=CARTESIAN_POINT('Ctrl Pts',(38.1203539798842,4.19279587918222,337.574574971823));
#65077=CARTESIAN_POINT('Ctrl Pts',(38.1125968701095,4.26124267164846,337.455808208273));
#65078=CARTESIAN_POINT('Ctrl Pts',(38.1048356151833,4.32972603989205,337.336977979563));
#65079=CARTESIAN_POINT('Ctrl Pts',(38.0970743602571,4.39318073164775,337.215375262923));
#65080=CARTESIAN_POINT('Ctrl Pts',(38.0893131053309,4.45139676410234,337.091470753092));
#65081=CARTESIAN_POINT('Ctrl Pts',(38.0815394349263,4.5097059232363,336.967368036426));
#65082=CARTESIAN_POINT('Ctrl Pts',(38.0737657645216,4.56275952570881,336.840956529214));
#65083=CARTESIAN_POINT('Ctrl Pts',(38.0659920941169,4.61039622212024,336.712725820895));
#65084=CARTESIAN_POINT('Ctrl Pts',(38.0585802899399,4.65581541885267,336.590464282899));
#65085=CARTESIAN_POINT('Ctrl Pts',(38.0511684857629,4.69631058480863,336.466549373467));
#65086=CARTESIAN_POINT('Ctrl Pts',(38.0437566815859,4.7317850272708,336.341414745034));
#65087=CARTESIAN_POINT('Ctrl Pts',(38.0359816028074,4.76899817783125,336.210146895705));
#65088=CARTESIAN_POINT('Ctrl Pts',(38.028206524029,4.800803599795,336.077121909416));
#65089=CARTESIAN_POINT('Ctrl Pts',(38.0204314452506,4.82703472166327,335.942824935159));
#65090=CARTESIAN_POINT('Ctrl Pts',(38.0126659342016,4.85323356446613,335.808693221878));
#65091=CARTESIAN_POINT('Ctrl Pts',(38.0049004231525,4.87387168145963,335.673293015009));
#65092=CARTESIAN_POINT('Ctrl Pts',(37.9971349121035,4.88883216852958,335.537124836933));
#65093=CARTESIAN_POINT('Ctrl Pts',(37.9893771005813,4.90377782223305,335.401091670002));
#65094=CARTESIAN_POINT('Ctrl Pts',(37.9816192890591,4.91305700639798,335.264292433218));
#65095=CARTESIAN_POINT('Ctrl Pts',(37.9738614775369,4.91660387119302,335.127237715595));
#65096=CARTESIAN_POINT('Ctrl Pts',(37.9661095040138,4.92014806685982,334.990286135993));
#65097=CARTESIAN_POINT('Ctrl Pts',(37.9583575304908,4.91796851939799,334.853079847402));
#65098=CARTESIAN_POINT('Ctrl Pts',(37.9506055569678,4.91005124228594,334.716134079844));
#65099=CARTESIAN_POINT('Ctrl Pts',(37.9428568664102,4.90213731814548,334.579246308899));
#65100=CARTESIAN_POINT('Ctrl Pts',(37.9351081758526,4.88849051983128,334.442619228958));
#65101=CARTESIAN_POINT('Ctrl Pts',(37.9273594852949,4.86914895864659,334.306767368764));
#65102=CARTESIAN_POINT('Ctrl Pts',(37.9196124069171,4.84981142163528,334.170943773683));
#65103=CARTESIAN_POINT('Ctrl Pts',(37.9118653285393,4.82478153354952,334.03589546426));
#65104=CARTESIAN_POINT('Ctrl Pts',(37.9041182501614,4.7941491614406,333.902130754435));
#65105=CARTESIAN_POINT('Ctrl Pts',(37.8963711068556,4.7635165326029,333.768364923532));
#65106=CARTESIAN_POINT('Ctrl Pts',(37.8886239635498,4.72728141334067,333.635883094698));
#65107=CARTESIAN_POINT('Ctrl Pts',(37.880876820244,4.68558448667703,333.505181923874));
#65108=CARTESIAN_POINT('Ctrl Pts',(37.8731279352159,4.64387818565897,333.374451368653));
#65109=CARTESIAN_POINT('Ctrl Pts',(37.8653790501878,4.59670775257178,333.245502640365));
#65110=CARTESIAN_POINT('Ctrl Pts',(37.8576301651597,4.54426316018289,333.118815428113));
#65111=CARTESIAN_POINT('Ctrl Pts',(37.849873055385,4.49176290256177,332.991993748745));
#65112=CARTESIAN_POINT('Ctrl Pts',(37.8421159456103,4.43397745275645,332.867438742153));
#65113=CARTESIAN_POINT('Ctrl Pts',(37.8343588358355,4.37114443438962,332.745608863528));
#65114=CARTESIAN_POINT('Ctrl Pts',(37.8265975809094,4.30827784006682,332.623713882911));
#65115=CARTESIAN_POINT('Ctrl Pts',(37.8188363259832,4.24035849610238,332.504547271331));
#65116=CARTESIAN_POINT('Ctrl Pts',(37.811075071057,4.16766858599533,332.388540327746));
#65117=CARTESIAN_POINT('Ctrl Pts',(37.8033014006524,4.0948623957217,332.272347810859));
#65118=CARTESIAN_POINT('Ctrl Pts',(37.7955277302477,4.01727061094869,332.159325384647));
#65119=CARTESIAN_POINT('Ctrl Pts',(37.787754059843,3.93521762246236,332.049873676203));
#65120=CARTESIAN_POINT('Ctrl Pts',(37.7803422556659,3.85698422033066,331.945516971118));
#65121=CARTESIAN_POINT('Ctrl Pts',(37.7729304514888,3.77469578729007,331.844406254409));
#65122=CARTESIAN_POINT('Ctrl Pts',(37.7655186473117,3.68866466494969,331.746857511259));
#65123=CARTESIAN_POINT('Ctrl Pts',(37.7577435685333,3.59841690103013,331.644527613625));
#65124=CARTESIAN_POINT('Ctrl Pts',(37.7499684897548,3.50376509091556,331.545794302704));
#65125=CARTESIAN_POINT('Ctrl Pts',(37.7421934109764,3.40502706534648,331.451060193979));
#65126=CARTESIAN_POINT('Ctrl Pts',(37.7344278999274,3.30641054320355,331.356442661606));
#65127=CARTESIAN_POINT('Ctrl Pts',(37.7266623888783,3.20371808993043,331.265814807532));
#65128=CARTESIAN_POINT('Ctrl Pts',(37.7188968778293,3.09730734195156,331.179545800302));
#65129=CARTESIAN_POINT('Ctrl Pts',(37.7111390663071,2.99100210053962,331.093362329043));
#65130=CARTESIAN_POINT('Ctrl Pts',(37.7033812547849,2.88098620283537,331.011529348554));
#65131=CARTESIAN_POINT('Ctrl Pts',(37.6956234432627,2.76765337891204,330.934378542375));
#65132=CARTESIAN_POINT('Ctrl Pts',(37.6878714697397,2.65440584153209,330.857285794625));
#65133=CARTESIAN_POINT('Ctrl Pts',(37.6801194962166,2.5378466680937,330.784868426932));
#65134=CARTESIAN_POINT('Ctrl Pts',(37.6723675226936,2.41840155760518,330.717417021391));
#65135=CARTESIAN_POINT('Ctrl Pts',(37.664618832136,2.2990070321922,330.64999418156));
#65136=CARTESIAN_POINT('Ctrl Pts',(37.6568701415783,2.17672934023772,330.587533312788));
#65137=CARTESIAN_POINT('Ctrl Pts',(37.6491214510207,2.05202178415196,330.530280807493));
#65138=CARTESIAN_POINT('Ctrl Pts',(37.6413743726429,1.92734017451499,330.47304021406));
#65139=CARTESIAN_POINT('Ctrl Pts',(37.6336272942651,1.80023006133307,330.421005991641));
#65140=CARTESIAN_POINT('Ctrl Pts',(37.6258802158872,1.67116752886275,330.374377646957));
#65141=CARTESIAN_POINT('Ctrl Pts',(37.6181330725814,1.54210391472391,330.327748911482));
#65142=CARTESIAN_POINT('Ctrl Pts',(37.6103859292756,1.41108821627704,330.286526276924));
#65143=CARTESIAN_POINT('Ctrl Pts',(37.6026387859698,1.27861421375738,330.250860208956));
#65144=CARTESIAN_POINT('Ctrl Pts',(37.5948899009417,1.14611042826981,330.215186122499));
#65145=CARTESIAN_POINT('Ctrl Pts',(37.5871410159136,1.01214806366985,330.185071190066));
#65146=CARTESIAN_POINT('Ctrl Pts',(37.5793921308855,0.877233305922503,330.160615246803));
#65147=CARTESIAN_POINT('Ctrl Pts',(37.5716350211108,0.742175348257355,330.136133345748));
#65148=CARTESIAN_POINT('Ctrl Pts',(37.5638779113361,0.606163363331336,330.117322502256));
#65149=CARTESIAN_POINT('Ctrl Pts',(37.5561208015613,0.46971146767299,330.104230989963));
#65150=CARTESIAN_POINT('Ctrl Pts',(37.5483595466352,0.333186656484583,330.091132481985));
#65151=CARTESIAN_POINT('Ctrl Pts',(37.5405982917091,0.196221856268451,330.083759416016));
#65152=CARTESIAN_POINT('Ctrl Pts',(37.5328370367829,0.0593324612038433,
330.082107898546));
#65153=CARTESIAN_POINT('Ctrl Pts',(37.5250633663782,-0.0777759122809043,
330.080453739186));
#65154=CARTESIAN_POINT('Ctrl Pts',(37.5172896959735,-0.214808248666145,
330.084539406301));
#65155=CARTESIAN_POINT('Ctrl Pts',(37.5095160255689,-0.351252105616479,
330.094308915066));
#65156=CARTESIAN_POINT('Ctrl Pts',(37.5021042213919,-0.481344468197614,
330.103623650848));
#65157=CARTESIAN_POINT('Ctrl Pts',(37.4946924172149,-0.610901619807047,
330.118104939194));
#65158=CARTESIAN_POINT('Ctrl Pts',(37.4872806130379,-0.739488815793786,
330.1376611231));
#65159=CARTESIAN_POINT('Ctrl Pts',(37.4795055342595,-0.874378453298963,
330.158175813833));
#65160=CARTESIAN_POINT('Ctrl Pts',(37.471730455481,-1.0086269264079,330.184340280411));
#65161=CARTESIAN_POINT('Ctrl Pts',(37.4639553767026,-1.14172367072025,330.216105130522));
#65162=CARTESIAN_POINT('Ctrl Pts',(37.4561898656536,-1.274656631015,330.247830891963));
#65163=CARTESIAN_POINT('Ctrl Pts',(37.4484243546047,-1.40644030592325,330.285143234703));
#65164=CARTESIAN_POINT('Ctrl Pts',(37.4406588435557,-1.53657071614992,330.327941192925));
#65165=CARTESIAN_POINT('Ctrl Pts',(37.4329010320335,-1.66657210169624,330.370696716846));
#65166=CARTESIAN_POINT('Ctrl Pts',(37.4251432205113,-1.79492311577844,330.418926910994));
#65167=CARTESIAN_POINT('Ctrl Pts',(37.4173854089891,-1.92113176869542,330.472480172345));
#65168=CARTESIAN_POINT('Ctrl Pts',(37.409633435466,-2.04724544559947,330.525993133169));
#65169=CARTESIAN_POINT('Ctrl Pts',(37.401881461943,-2.17121961196057,330.584821035828));
#65170=CARTESIAN_POINT('Ctrl Pts',(37.3941294884199,-2.29257954093718,330.648763151588));
#65171=CARTESIAN_POINT('Ctrl Pts',(37.3863807978623,-2.41388807391132,330.712678187824));
#65172=CARTESIAN_POINT('Ctrl Pts',(37.3786321073047,-2.53258422641506,330.781702947572));
#65173=CARTESIAN_POINT('Ctrl Pts',(37.370883416747,-2.64821549386231,330.85558957624));
#65174=CARTESIAN_POINT('Ctrl Pts',(37.3631363383692,-2.7638227032586,330.929460832178));
#65175=CARTESIAN_POINT('Ctrl Pts',(37.3553892599913,-2.87636596681179,331.008191734654));
#65176=CARTESIAN_POINT('Ctrl Pts',(37.3476421816135,-2.98541987855531,331.091489898794));
#65177=CARTESIAN_POINT('Ctrl Pts',(37.3398950383077,-3.09447470427565,331.174788761053));
#65178=CARTESIAN_POINT('Ctrl Pts',(37.332147895002,-3.20003980923074,331.262654724061));
#65179=CARTESIAN_POINT('Ctrl Pts',(37.3244007516961,-3.30172145080692,331.354753983092));
#65180=CARTESIAN_POINT('Ctrl Pts',(37.3166518666681,-3.40342595257434,331.446873947992));
#65181=CARTESIAN_POINT('Ctrl Pts',(37.30890298164,-3.50124496397462,331.543228840412));
#65182=CARTESIAN_POINT('Ctrl Pts',(37.3011540966119,-3.59482060523396,331.643447024299));
#65183=CARTESIAN_POINT('Ctrl Pts',(37.2933969868372,-3.68849556864625,331.743771580803));
#65184=CARTESIAN_POINT('Ctrl Pts',(37.2856398770624,-3.77791789766018,331.847967333836));
#65185=CARTESIAN_POINT('Ctrl Pts',(37.2778827672877,-3.86276877999129,331.955628075477));
#65186=CARTESIAN_POINT('Ctrl Pts',(37.2701215123615,-3.94766500392096,332.063346347575));
#65187=CARTESIAN_POINT('Ctrl Pts',(37.2623602574353,-4.02798468482792,332.174532981031));
#65188=CARTESIAN_POINT('Ctrl Pts',(37.2545990025092,-4.10345218748378,332.288752462881));
#65189=CARTESIAN_POINT('Ctrl Pts',(37.2468253321045,-4.17904041354899,332.403154658678));
#65190=CARTESIAN_POINT('Ctrl Pts',(37.2390516616998,-4.2497607490397,332.520599062712));
#65191=CARTESIAN_POINT('Ctrl Pts',(37.2312779912952,-4.31538296083877,332.640624454691));
#65192=CARTESIAN_POINT('Ctrl Pts',(37.2238661871181,-4.37795044289079,332.755062635796));
#65193=CARTESIAN_POINT('Ctrl Pts',(37.216454382941,-4.43588362729956,332.871846664628));
#65194=CARTESIAN_POINT('Ctrl Pts',(37.2090425787639,-4.48902432512157,332.990561354267));
#65195=CARTESIAN_POINT('Ctrl Pts',(37.2005133259487,-4.55017683747444,333.127174191925));
#65196=CARTESIAN_POINT('Ctrl Pts',(37.1919840731336,-4.60515010793779,333.266716439433));
#65197=CARTESIAN_POINT('Ctrl Pts',(37.1834548203184,-4.65368063737661,333.408635934864));
#65198=CARTESIAN_POINT('Ctrl Pts',(37.174957512741,-4.70202940185503,333.550023888773));
#65199=CARTESIAN_POINT('Ctrl Pts',(37.1664602051637,-4.74398346463822,333.693771082907));
#65200=CARTESIAN_POINT('Ctrl Pts',(37.1579628975863,-4.7793279453148,333.839307338856));
#65201=CARTESIAN_POINT('Ctrl Pts',(37.1494858615255,-4.81458810678542,333.984496397695));
#65202=CARTESIAN_POINT('Ctrl Pts',(37.1410088254647,-4.84327005782944,334.131465754266));
#65203=CARTESIAN_POINT('Ctrl Pts',(37.1325317894039,-4.86520793403035,334.279628692168));
#65204=CARTESIAN_POINT('Ctrl Pts',(37.1240869843794,-4.88706239894484,334.427228291069));
#65205=CARTESIAN_POINT('Ctrl Pts',(37.1156421793548,-4.9022238761433,334.576012161315));
#65206=CARTESIAN_POINT('Ctrl Pts',(37.1071973743303,-4.91057723754466,334.72538343712));
#65207=CARTESIAN_POINT('Ctrl Pts',(37.1020707084038,-4.91564838994467,334.816063639663));
#65208=CARTESIAN_POINT('Ctrl Pts',(37.0969440424774,-4.91821139877864,334.906960017087));
#65209=CARTESIAN_POINT('Ctrl Pts',(37.0918173765509,-4.91824956715858,334.997936593961));
#65210=CARTESIAN_POINT('',(35.34181657491,-4.91667364108997,335.004349070568));
#65211=CARTESIAN_POINT('Ctrl Pts',(37.0918173765087,-4.91824956715889,334.99793659471));
#65212=CARTESIAN_POINT('Ctrl Pts',(37.0839206660765,-4.91830835868908,335.138069713192));
#65213=CARTESIAN_POINT('Ctrl Pts',(37.0760239556444,-4.91237368761718,335.278174596858));
#65214=CARTESIAN_POINT('Ctrl Pts',(37.0681272452122,-4.90047919903303,335.417716030749));
#65215=CARTESIAN_POINT('Ctrl Pts',(37.0602271166153,-4.88857956180854,335.557317866451));
#65216=CARTESIAN_POINT('Ctrl Pts',(37.0523269880183,-4.87071499803595,335.696355398293));
#65217=CARTESIAN_POINT('Ctrl Pts',(37.0444268594214,-4.84697094239054,335.83429955419));
#65218=CARTESIAN_POINT('Ctrl Pts',(37.0365218817839,-4.82321231281928,335.97232837919));
#65219=CARTESIAN_POINT('Ctrl Pts',(37.0286169041465,-4.7935670632542,336.109262127297));
#65220=CARTESIAN_POINT('Ctrl Pts',(37.020711926509,-4.75817151016775,336.244583039547));
#65221=CARTESIAN_POINT('Ctrl Pts',(37.0127949002831,-4.72272200797866,336.380110204876));
#65222=CARTESIAN_POINT('Ctrl Pts',(37.0048778740573,-4.68150478494827,336.514019265025));
#65223=CARTESIAN_POINT('Ctrl Pts',(36.9969608478314,-4.63470602834046,336.645807732806));
#65224=CARTESIAN_POINT('Ctrl Pts',(36.9890374299877,-4.5878694898993,336.777702596789));
#65225=CARTESIAN_POINT('Ctrl Pts',(36.9811140121441,-4.53544257188891,336.907473113106));
#65226=CARTESIAN_POINT('Ctrl Pts',(36.9731905943004,-4.47765897625038,337.03463833516));
#65227=CARTESIAN_POINT('Ctrl Pts',(36.9652525752252,-4.41976889731394,337.162037896599));
#65228=CARTESIAN_POINT('Ctrl Pts',(36.95731455615,-4.35650257943818,337.286822239184));
#65229=CARTESIAN_POINT('Ctrl Pts',(36.9493765370747,-4.288139472326,337.408535432245));
#65230=CARTESIAN_POINT('Ctrl Pts',(36.9431858728799,-4.23482478065828,337.503456532734));
#65231=CARTESIAN_POINT('Ctrl Pts',(36.9369952086849,-4.17841111909408,337.596510255459));
#65232=CARTESIAN_POINT('Ctrl Pts',(36.9308045444901,-4.11904846917579,337.687493771357));
#65233=CARTESIAN_POINT('Ctrl Pts',(36.9230294657116,-4.04449277287554,337.801763255434));
#65234=CARTESIAN_POINT('Ctrl Pts',(36.9152543869332,-3.96506061343784,337.913108501809));
#65235=CARTESIAN_POINT('Ctrl Pts',(36.9074793081548,-3.88100847035088,338.021085287701));
#65236=CARTESIAN_POINT('Ctrl Pts',(36.8997137971058,-3.7970597587769,338.128929201284));
#65237=CARTESIAN_POINT('Ctrl Pts',(36.8919482860568,-3.70850261324296,338.233412596463));
#65238=CARTESIAN_POINT('Ctrl Pts',(36.8841827750078,-3.61563772423811,338.334118610603));
#65239=CARTESIAN_POINT('Ctrl Pts',(36.8764249634856,-3.52286491104113,338.434724774436));
#65240=CARTESIAN_POINT('Ctrl Pts',(36.8686671519634,-3.42579311745344,338.531560725059));
#65241=CARTESIAN_POINT('Ctrl Pts',(36.8609093404412,-3.32476415373212,338.624241490927));
#65242=CARTESIAN_POINT('Ctrl Pts',(36.8531573669182,-3.2238112175098,338.71685251158));
#65243=CARTESIAN_POINT('Ctrl Pts',(36.8454053933952,-3.11890732538444,338.805314308266));
#65244=CARTESIAN_POINT('Ctrl Pts',(36.8376534198722,-3.01043184700796,338.88927797374));
#65245=CARTESIAN_POINT('Ctrl Pts',(36.8299047293146,-2.90200230806113,338.973206080552));
#65246=CARTESIAN_POINT('Ctrl Pts',(36.822156038757,-2.79000449971037,339.052639606232));
#65247=CARTESIAN_POINT('Ctrl Pts',(36.8144073481994,-2.67485147618795,339.127269393053));
#65248=CARTESIAN_POINT('Ctrl Pts',(36.8066602698216,-2.55972241121386,339.201883652524));
#65249=CARTESIAN_POINT('Ctrl Pts',(36.7989131914438,-2.44143976463688,339.27169594868));
#65250=CARTESIAN_POINT('Ctrl Pts',(36.7911661130659,-2.32044589266319,339.336440236152));
#65251=CARTESIAN_POINT('Ctrl Pts',(36.7834189697601,-2.19945100664414,339.401185066245));
#65252=CARTESIAN_POINT('Ctrl Pts',(36.7756718264544,-2.07574519454169,339.46086161852));
#65253=CARTESIAN_POINT('Ctrl Pts',(36.7679246831486,-1.94979539244553,339.515249825879));
#65254=CARTESIAN_POINT('Ctrl Pts',(36.7601757981205,-1.82381727416021,339.569650260861));
#65255=CARTESIAN_POINT('Ctrl Pts',(36.7524269130924,-1.69559452076537,339.618759830157));
#65256=CARTESIAN_POINT('Ctrl Pts',(36.7446780280643,-1.56561364233383,339.662406780348));
#65257=CARTESIAN_POINT('Ctrl Pts',(36.7369209182896,-1.43549480085479,339.706100057864));
#65258=CARTESIAN_POINT('Ctrl Pts',(36.7291638085149,-1.30361447777166,339.744319009443));
#65259=CARTESIAN_POINT('Ctrl Pts',(36.7214066987401,-1.17047446289557,339.776941761651));
#65260=CARTESIAN_POINT('Ctrl Pts',(36.713645443814,-1.03726330225261,339.809581946415));
#65261=CARTESIAN_POINT('Ctrl Pts',(36.7058841888879,-0.902791491537083,
339.836619896095));
#65262=CARTESIAN_POINT('Ctrl Pts',(36.6981229339617,-0.767569604154022,
339.85798517549));
#65263=CARTESIAN_POINT('Ctrl Pts',(36.6903492635571,-0.632131405819857,
339.879384632369));
#65264=CARTESIAN_POINT('Ctrl Pts',(36.6825755931524,-0.495941121610227,
339.895093240766));
#65265=CARTESIAN_POINT('Ctrl Pts',(36.6748019227477,-0.359513912265738,
339.90509253831));
#65266=CARTESIAN_POINT('Ctrl Pts',(36.6673901185705,-0.229437422335778,
339.914626366148));
#65267=CARTESIAN_POINT('Ctrl Pts',(36.6599783143933,-0.0991458562419824,
339.918970448477));
#65268=CARTESIAN_POINT('Ctrl Pts',(36.652566510216,0.0309173698767789,339.918152821816));
#65269=CARTESIAN_POINT('Ctrl Pts',(36.6447914314376,0.167355382142981,339.917295120837));
#65270=CARTESIAN_POINT('Ctrl Pts',(36.6370163526592,0.30397327455472,339.910754225158));
#65271=CARTESIAN_POINT('Ctrl Pts',(36.6292412738808,0.440258694930354,339.898505419415));
#65272=CARTESIAN_POINT('Ctrl Pts',(36.6214757628317,0.57637640742023,339.886271686607));
#65273=CARTESIAN_POINT('Ctrl Pts',(36.6137102517827,0.712162076337915,339.868344054031));
#65274=CARTESIAN_POINT('Ctrl Pts',(36.6059447407337,0.847102432123598,339.844749790442));
#65275=CARTESIAN_POINT('Ctrl Pts',(36.5981869292115,0.981908994153377,339.821178920635));
#65276=CARTESIAN_POINT('Ctrl Pts',(36.5904291176893,1.11587152842548,339.791952667799));
#65277=CARTESIAN_POINT('Ctrl Pts',(36.5826713061672,1.24848133101156,339.757150137279));
#65278=CARTESIAN_POINT('Ctrl Pts',(36.5749193326442,1.38099134051589,339.722373796768));
#65279=CARTESIAN_POINT('Ctrl Pts',(36.5671673591212,1.51215026801197,339.682029629977));
#65280=CARTESIAN_POINT('Ctrl Pts',(36.5594153855982,1.64145941126676,339.636247843209));
#65281=CARTESIAN_POINT('Ctrl Pts',(36.5516666950406,1.77071379202244,339.590485445056));
#65282=CARTESIAN_POINT('Ctrl Pts',(36.5439180044829,1.8981195789383,339.539290137286));
#65283=CARTESIAN_POINT('Ctrl Pts',(36.5361693139253,2.02319326733982,339.482841963029));
#65284=CARTESIAN_POINT('Ctrl Pts',(36.5284222355475,2.14824093311601,339.426405533286));
#65285=CARTESIAN_POINT('Ctrl Pts',(36.5206751571697,2.27095710945309,339.364718571608));
#65286=CARTESIAN_POINT('Ctrl Pts',(36.5129280787919,2.39087868879991,339.298009092352));
#65287=CARTESIAN_POINT('Ctrl Pts',(36.5051809354861,2.5108012732049,339.231299054007));
#65288=CARTESIAN_POINT('Ctrl Pts',(36.4974337921803,2.62792887232276,339.159566604138));
#65289=CARTESIAN_POINT('Ctrl Pts',(36.4896866488745,2.74182374112443,339.083085308331));
#65290=CARTESIAN_POINT('Ctrl Pts',(36.4819377638464,2.85574421591082,339.006586817904));
#65291=CARTESIAN_POINT('Ctrl Pts',(36.4741888788183,2.96643018972047,338.925337574914));
#65292=CARTESIAN_POINT('Ctrl Pts',(36.4664399937902,3.07347395292423,338.839653750431));
#65293=CARTESIAN_POINT('Ctrl Pts',(36.4586828840155,3.18063133348421,338.75387898025));
#65294=CARTESIAN_POINT('Ctrl Pts',(36.4509257742408,3.28413847534477,338.663660470729));
#65295=CARTESIAN_POINT('Ctrl Pts',(36.4431686644661,3.38362134527426,338.569354234915));
#65296=CARTESIAN_POINT('Ctrl Pts',(36.4354074095399,3.48315737566853,338.474997604864));
#65297=CARTESIAN_POINT('Ctrl Pts',(36.4276461546138,3.57866457715264,338.376549176411));
#65298=CARTESIAN_POINT('Ctrl Pts',(36.4198848996876,3.6698074186975,338.274400185098));
#65299=CARTESIAN_POINT('Ctrl Pts',(36.412111229283,3.76109605908532,338.17208778869));
#65300=CARTESIAN_POINT('Ctrl Pts',(36.4043375588784,3.84800614039774,338.066063302569));
#65301=CARTESIAN_POINT('Ctrl Pts',(36.3965638884737,3.9302433541959,337.956749945345));
#65302=CARTESIAN_POINT('Ctrl Pts',(36.3891520842966,4.00865240590784,337.852525151198));
#65303=CARTESIAN_POINT('Ctrl Pts',(36.3817402801194,4.08281367995659,337.745311025833));
#65304=CARTESIAN_POINT('Ctrl Pts',(36.3743284759422,4.15251079493285,337.635495619512));
#65305=CARTESIAN_POINT('Ctrl Pts',(36.3665533971637,4.22562397313061,337.520297833004));
#65306=CARTESIAN_POINT('Ctrl Pts',(36.3587783183852,4.2940553751274,337.401873278691));
#65307=CARTESIAN_POINT('Ctrl Pts',(36.3510032396068,4.35750695408287,337.28063942955));
#65308=CARTESIAN_POINT('Ctrl Pts',(36.3432377285577,4.42088045183075,337.15955476638));
#65309=CARTESIAN_POINT('Ctrl Pts',(36.3354722175087,4.47928613995949,337.035668029852));
#65310=CARTESIAN_POINT('Ctrl Pts',(36.3277067064597,4.53246918973772,336.909425595979));
#65311=CARTESIAN_POINT('Ctrl Pts',(36.3199488949374,4.58559950836736,336.783308331846));
#65312=CARTESIAN_POINT('Ctrl Pts',(36.3121910834152,4.63351734290625,336.654840376399));
#65313=CARTESIAN_POINT('Ctrl Pts',(36.3044332718929,4.67601392584138,336.524492318064));
#65314=CARTESIAN_POINT('Ctrl Pts',(36.2966812983699,4.71847852875002,336.394242350778));
#65315=CARTESIAN_POINT('Ctrl Pts',(36.2889293248469,4.75552987975614,336.262115466895));
#65316=CARTESIAN_POINT('Ctrl Pts',(36.2811773513239,4.78700759572399,336.128601497864));
#65317=CARTESIAN_POINT('Ctrl Pts',(36.2734286607663,4.81847198086049,335.995144072078));
#65318=CARTESIAN_POINT('Ctrl Pts',(36.2656799702086,4.84436733619497,335.860301109156));
#65319=CARTESIAN_POINT('Ctrl Pts',(36.257931279651,4.86458341171398,335.724576630162));
#65320=CARTESIAN_POINT('Ctrl Pts',(36.2501842012731,4.88479528110962,335.58888038978));
#65321=CARTESIAN_POINT('Ctrl Pts',(36.2424371228952,4.89933016346967,335.452303384502));
#65322=CARTESIAN_POINT('Ctrl Pts',(36.2346900445174,4.90812918686222,335.315358443));
#65323=CARTESIAN_POINT('Ctrl Pts',(36.2269429012115,4.91692828399907,335.178412353767));
#65324=CARTESIAN_POINT('Ctrl Pts',(36.2191957579057,4.91999140122227,335.041098712229));
#65325=CARTESIAN_POINT('Ctrl Pts',(36.2114486145999,4.91731169671548,334.903933669555));
#65326=CARTESIAN_POINT('Ctrl Pts',(36.2036997295718,4.91463138975423,334.766737789268));
#65327=CARTESIAN_POINT('Ctrl Pts',(36.1959508445437,4.90620569953516,334.629690965047));
#65328=CARTESIAN_POINT('Ctrl Pts',(36.1882019595155,4.89207986598166,334.493307146925));
#65329=CARTESIAN_POINT('Ctrl Pts',(36.1804448497408,4.87793903912246,334.35677856961));
#65330=CARTESIAN_POINT('Ctrl Pts',(36.172687739966,4.85808602343729,334.220914793552));
#65331=CARTESIAN_POINT('Ctrl Pts',(36.1649306301912,4.83261778704999,334.086223010364));
#65332=CARTESIAN_POINT('Ctrl Pts',(36.157169375265,4.80713594125147,333.951459252194));
#65333=CARTESIAN_POINT('Ctrl Pts',(36.1494081203388,4.77603298438545,333.817869115303));
#65334=CARTESIAN_POINT('Ctrl Pts',(36.1416468654126,4.73945633967175,333.685946474893));
#65335=CARTESIAN_POINT('Ctrl Pts',(36.1338731950079,4.7028211842468,333.553812801252));
#65336=CARTESIAN_POINT('Ctrl Pts',(36.1260995246033,4.6606949638316,333.423352326607));
#65337=CARTESIAN_POINT('Ctrl Pts',(36.1183258541986,4.61327430479938,333.295041569076));
#65338=CARTESIAN_POINT('Ctrl Pts',(36.1109140500217,4.56806108885559,333.172703708183));
#65339=CARTESIAN_POINT('Ctrl Pts',(36.1035022458449,4.51803536428646,333.0523201955));
#65340=CARTESIAN_POINT('Ctrl Pts',(36.0960904416681,4.46340635443777,332.934282987032));
#65341=CARTESIAN_POINT('Ctrl Pts',(36.0883153628896,4.40609981408298,332.810460423358));
#65342=CARTESIAN_POINT('Ctrl Pts',(36.0805402841112,4.34354623809749,332.688828675961));
#65343=CARTESIAN_POINT('Ctrl Pts',(36.0727652053328,4.27593539816851,332.569864297372));
#65344=CARTESIAN_POINT('Ctrl Pts',(36.0649996942838,4.20840775768237,332.451046312023));
#65345=CARTESIAN_POINT('Ctrl Pts',(36.0572341832348,4.13583542709292,332.334889501091));
#65346=CARTESIAN_POINT('Ctrl Pts',(36.0494686721858,4.05845587106273,332.221849715164));
#65347=CARTESIAN_POINT('Ctrl Pts',(36.0417108606636,3.98115303708789,332.108922008514));
#65348=CARTESIAN_POINT('Ctrl Pts',(36.0339530491414,3.89905268240325,331.999105496987));
#65349=CARTESIAN_POINT('Ctrl Pts',(36.0261952376192,3.81243755877643,331.892830400038));
#65350=CARTESIAN_POINT('Ctrl Pts',(36.0184432640962,3.72588761577616,331.786635278468));
#65351=CARTESIAN_POINT('Ctrl Pts',(36.0106912905731,3.63482991235051,331.683976568643));
#65352=CARTESIAN_POINT('Ctrl Pts',(36.00293931705,3.53958956569751,331.585254216065));
#65353=CARTESIAN_POINT('Ctrl Pts',(35.9951906264924,3.44438955338826,331.486573672462));
#65354=CARTESIAN_POINT('Ctrl Pts',(35.9874419359348,3.34501069176538,331.391826451183));
#65355=CARTESIAN_POINT('Ctrl Pts',(35.9796932453771,3.24181716028654,331.301378018536));
#65356=CARTESIAN_POINT('Ctrl Pts',(35.9719461669993,3.13864509908395,331.21094840444));
#65357=CARTESIAN_POINT('Ctrl Pts',(35.9641990886215,3.03166024045969,331.124816057433));
#65358=CARTESIAN_POINT('Ctrl Pts',(35.9564520102437,2.92126197400406,331.043308005197));
#65359=CARTESIAN_POINT('Ctrl Pts',(35.9487048669378,2.81086278230462,330.961799269845));
#65360=CARTESIAN_POINT('Ctrl Pts',(35.9409577236321,2.6970504401689,330.884915138733));
#65361=CARTESIAN_POINT('Ctrl Pts',(35.9332105803263,2.58025528762715,330.812940684302));
#65362=CARTESIAN_POINT('Ctrl Pts',(35.9254616952982,2.46343387705549,330.740950048486));
#65363=CARTESIAN_POINT('Ctrl Pts',(35.9177128102701,2.34362865435892,330.673871490815));
#65364=CARTESIAN_POINT('Ctrl Pts',(35.909963925242,2.22129629300343,330.611945095924));
#65365=CARTESIAN_POINT('Ctrl Pts',(35.9022068154673,2.09883408681583,330.549952971717));
#65366=CARTESIAN_POINT('Ctrl Pts',(35.8944497056925,1.97383973304959,330.493124111066));
#65367=CARTESIAN_POINT('Ctrl Pts',(35.8866925959178,1.84679221496803,330.441651441889));
#65368=CARTESIAN_POINT('Ctrl Pts',(35.8789313409916,1.71967680675508,330.390151267364));
#65369=CARTESIAN_POINT('Ctrl Pts',(35.8711700860655,1.59050641597652,330.344013118873));
#65370=CARTESIAN_POINT('Ctrl Pts',(35.8634088311393,1.45977613198823,330.303380289296));
#65371=CARTESIAN_POINT('Ctrl Pts',(35.8556351607347,1.32883672215045,330.262682460433));
#65372=CARTESIAN_POINT('Ctrl Pts',(35.84786149033,1.19633281070121,330.227507649253));
#65373=CARTESIAN_POINT('Ctrl Pts',(35.8400878199253,1.06277151770532,330.197948379739));
#65374=CARTESIAN_POINT('Ctrl Pts',(35.8326760157483,0.935427535032283,330.169765101332));
#65375=CARTESIAN_POINT('Ctrl Pts',(35.8252642115713,0.807122680904278,330.146686374056));
#65376=CARTESIAN_POINT('Ctrl Pts',(35.8178524073943,0.67829978224585,330.128748367421));
#65377=CARTESIAN_POINT('Ctrl Pts',(35.8100773286159,0.5431628895795,330.109931165645));
#65378=CARTESIAN_POINT('Ctrl Pts',(35.8023022498374,0.407028829004848,330.096711884469));
#65379=CARTESIAN_POINT('Ctrl Pts',(35.794527171059,0.270401040060297,330.08918883075));
#65380=CARTESIAN_POINT('Ctrl Pts',(35.78676166001,0.133941380308749,330.081675034627));
#65381=CARTESIAN_POINT('Ctrl Pts',(35.7789961489611,-0.00301041238201688,
330.07984354021));
#65382=CARTESIAN_POINT('Ctrl Pts',(35.7712306379121,-0.139942497771345,
330.08374134531));
#65383=CARTESIAN_POINT('Ctrl Pts',(35.7634728263899,-0.276738814600179,
330.087635285724));
#65384=CARTESIAN_POINT('Ctrl Pts',(35.7557150148676,-0.413515074813833,
330.097247209855));
#65385=CARTESIAN_POINT('Ctrl Pts',(35.7479572033454,-0.549756484487828,
330.112572162143));
#65386=CARTESIAN_POINT('Ctrl Pts',(35.7402052298225,-0.685895368179283,
330.127885581917));
#65387=CARTESIAN_POINT('Ctrl Pts',(35.7324532562995,-0.821499815610984,
330.148903428916));
#65388=CARTESIAN_POINT('Ctrl Pts',(35.7247012827766,-0.956057564505091,
330.175568738613));
#65389=CARTESIAN_POINT('Ctrl Pts',(35.716952592219,-1.09055832811339,330.202222755534));
#65390=CARTESIAN_POINT('Ctrl Pts',(35.7092039016614,-1.22401289221155,330.234519402399));
#65391=CARTESIAN_POINT('Ctrl Pts',(35.7014552111038,-1.35591684998379,330.272350207722));
#65392=CARTESIAN_POINT('Ctrl Pts',(35.6937081327259,-1.4877933640363,330.310173142029));
#65393=CARTESIAN_POINT('Ctrl Pts',(35.6859610543481,-1.61811953797953,330.353527836829));
#65394=CARTESIAN_POINT('Ctrl Pts',(35.6782139759703,-1.74640423463299,330.402255410339));
#65395=CARTESIAN_POINT('Ctrl Pts',(35.6704668326645,-1.87469000643559,330.450983392233));
#65396=CARTESIAN_POINT('Ctrl Pts',(35.6627196893587,-2.00093390141979,330.505084203859));
#65397=CARTESIAN_POINT('Ctrl Pts',(35.6549725460529,-2.1246633144027,330.564350232161));
#65398=CARTESIAN_POINT('Ctrl Pts',(35.6472236610248,-2.248420544384,330.623629584724));
#65399=CARTESIAN_POINT('Ctrl Pts',(35.6394747759968,-2.3696618150113,330.688076295898));
#65400=CARTESIAN_POINT('Ctrl Pts',(35.6317258909687,-2.48793810177526,330.757436262796));
#65401=CARTESIAN_POINT('Ctrl Pts',(35.623968781194,-2.60633992821235,330.82686984908));
#65402=CARTESIAN_POINT('Ctrl Pts',(35.6162116714193,-2.72177014652231,330.901226910462));
#65403=CARTESIAN_POINT('Ctrl Pts',(35.6084545616446,-2.83380731417333,330.980209064063));
#65404=CARTESIAN_POINT('Ctrl Pts',(35.6006933067184,-2.94590435090457,331.059233423203));
#65405=CARTESIAN_POINT('Ctrl Pts',(35.5929320517923,-3.05460441453063,331.142887560983));
#65406=CARTESIAN_POINT('Ctrl Pts',(35.5851707968661,-3.15951908575393,331.230832690201));
#65407=CARTESIAN_POINT('Ctrl Pts',(35.5773971264615,-3.26460158625944,331.318918502965));
#65408=CARTESIAN_POINT('Ctrl Pts',(35.5696234560568,-3.36588630496086,331.411308760289));
#65409=CARTESIAN_POINT('Ctrl Pts',(35.5618497856522,-3.4630210047002,331.50762708413));
#65410=CARTESIAN_POINT('Ctrl Pts',(35.5544379814749,-3.55563406079991,331.599461766825));
#65411=CARTESIAN_POINT('Ctrl Pts',(35.5470261772976,-3.64447457363195,331.694866832342));
#65412=CARTESIAN_POINT('Ctrl Pts',(35.5396143731203,-3.72927248842552,331.79348947147));
#65413=CARTESIAN_POINT('Ctrl Pts',(35.5318949702201,-3.81758961793084,331.896205067876));
#65414=CARTESIAN_POINT('Ctrl Pts',(35.5241755673199,-3.90181143064435,332.002748566461));
#65415=CARTESIAN_POINT('Ctrl Pts',(35.5164561644196,-3.98158401450764,332.112757059422));
#65416=CARTESIAN_POINT('Ctrl Pts',(35.5087491506717,-4.06122856843044,332.222588995725));
#65417=CARTESIAN_POINT('Ctrl Pts',(35.5010421369238,-4.13643788138174,332.335874534719));
#65418=CARTESIAN_POINT('Ctrl Pts',(35.4933351231759,-4.20689668647199,332.452215995841));
#65419=CARTESIAN_POINT('Ctrl Pts',(35.485635267547,-4.27729005084497,332.56844940136));
#65420=CARTESIAN_POINT('Ctrl Pts',(35.477935411918,-4.3429414775011,332.687732747526));
#65421=CARTESIAN_POINT('Ctrl Pts',(35.470235556289,-4.40357747833596,332.809637369112));
#65422=CARTESIAN_POINT('Ctrl Pts',(35.4625411241838,-4.46417076917623,332.931456125111));
#65423=CARTESIAN_POINT('Ctrl Pts',(35.4548466920786,-4.51975548521717,333.055892129898));
#65424=CARTESIAN_POINT('Ctrl Pts',(35.4471522599734,-4.57010304589883,333.182490381768));
#65425=CARTESIAN_POINT('Ctrl Pts',(35.4394615211818,-4.62042643984248,333.309027866706));
#65426=CARTESIAN_POINT('Ctrl Pts',(35.4317707823901,-4.66551753426074,333.437725165319));
#65427=CARTESIAN_POINT('Ctrl Pts',(35.4240800435984,-4.70519525290871,333.568105906673));
#65428=CARTESIAN_POINT('Ctrl Pts',(35.4163898424677,-4.74487019768002,333.698477533085));
#65429=CARTESIAN_POINT('Ctrl Pts',(35.408699641337,-4.77913239507231,333.830531991193));
#65430=CARTESIAN_POINT('Ctrl Pts',(35.4010094402063,-4.80785023672204,333.963776489481));
#65431=CARTESIAN_POINT('Ctrl Pts',(35.3933196499584,-4.83656654399476,334.097013868596));
#65432=CARTESIAN_POINT('Ctrl Pts',(35.3856298597104,-4.85973900678302,334.231440772012));
#65433=CARTESIAN_POINT('Ctrl Pts',(35.3779400694625,-4.87728703847865,334.366553706469));
#65434=CARTESIAN_POINT('Ctrl Pts',(35.3702464555423,-4.89484379575984,334.501733824499));
#65435=CARTESIAN_POINT('Ctrl Pts',(35.3625528416222,-4.90677048988907,334.637600260297));
#65436=CARTESIAN_POINT('Ctrl Pts',(35.354859227702,-4.91303836375677,334.773643867425));
#65437=CARTESIAN_POINT('Ctrl Pts',(35.3505119439709,-4.9165800317396,334.850515434691));
#65438=CARTESIAN_POINT('Ctrl Pts',(35.3461646602398,-4.91831588271506,334.927443513891));
#65439=CARTESIAN_POINT('Ctrl Pts',(35.3418173765088,-4.91824808840549,335.004336288243));
#65440=CARTESIAN_POINT('',(33.5918173765087,-4.92635458438153,334.999985596072));
#65441=CARTESIAN_POINT('Ctrl Pts',(35.3418159898256,-4.91552445706615,335.004358400345));
#65442=CARTESIAN_POINT('Ctrl Pts',(35.3150027728325,-4.91951882428191,335.478359568893));
#65443=CARTESIAN_POINT('Ctrl Pts',(35.1954435444147,-4.63874791474335,337.587276797197));
#65444=CARTESIAN_POINT('Ctrl Pts',(34.9831383045724,-1.62400073114428,340.584538520919));
#65445=CARTESIAN_POINT('Ctrl Pts',(34.7049002702985,3.81731760238167,339.387771095783));
#65446=CARTESIAN_POINT('Ctrl Pts',(34.4266622360246,5.75553991572094,334.164410899434));
#65447=CARTESIAN_POINT('Ctrl Pts',(34.1484242017505,2.41198820003029,329.707858487404));
#65448=CARTESIAN_POINT('Ctrl Pts',(33.9629321789013,-1.29267692394935,329.974503648868));
#65449=CARTESIAN_POINT('Ctrl Pts',(33.7773965704874,-4.03594356099226,331.738054986346));
#65450=CARTESIAN_POINT('Ctrl Pts',(33.684606973498,-4.92642524185015,333.368987177956));
#65451=CARTESIAN_POINT('Ctrl Pts',(33.5918173765087,-4.92635458438153,334.999985596072));
#65452=CARTESIAN_POINT('',(31.8418181870771,-4.91665217595445,334.995658470632));
#65453=CARTESIAN_POINT('Ctrl Pts',(33.5918173765087,-4.92635458438153,334.999985596072));
#65454=CARTESIAN_POINT('Ctrl Pts',(33.4991149506488,-4.92628399329202,336.629451773736));
#65455=CARTESIAN_POINT('Ctrl Pts',(33.3136665133641,-3.14873109843668,339.889282125032));
#65456=CARTESIAN_POINT('Ctrl Pts',(33.0354720646549,2.40701815814295,340.294403880779));
#65457=CARTESIAN_POINT('Ctrl Pts',(32.7572340303809,5.75475281454385,335.840992812056));
#65458=CARTESIAN_POINT('Ctrl Pts',(32.478995996107,3.82143575305017,330.615815052746));
#65459=CARTESIAN_POINT('Ctrl Pts',(32.200757961833,-1.61875649471839,329.413939109063));
#65460=CARTESIAN_POINT('Ctrl Pts',(31.9883655570254,-4.63755548700006,332.409598265075));
#65461=CARTESIAN_POINT('Ctrl Pts',(31.8687191636425,-4.91947903470235,334.520096393768));
#65462=CARTESIAN_POINT('Ctrl Pts',(31.8418187816841,-4.91548146079034,334.995648989438));
#65463=CARTESIAN_POINT('',(30.0918173764651,-4.91824955753923,335.002086208329));
#65464=CARTESIAN_POINT('Ctrl Pts',(31.8418173765087,-4.91824809517395,334.995671395399));
#65465=CARTESIAN_POINT('Ctrl Pts',(31.8341227429724,-4.91836788126847,335.131774778698));
#65466=CARTESIAN_POINT('Ctrl Pts',(31.8264281094361,-4.91283380696339,335.267987972518));
#65467=CARTESIAN_POINT('Ctrl Pts',(31.8187334758998,-4.90164537475895,335.403801538635));
#65468=CARTESIAN_POINT('Ctrl Pts',(31.8110415252819,-4.89046084366948,335.539567750098));
#65469=CARTESIAN_POINT('Ctrl Pts',(31.8033495746639,-4.87362590555103,335.674934215789));
#65470=CARTESIAN_POINT('Ctrl Pts',(31.7956576240459,-4.85119212798663,335.809393600086));
#65471=CARTESIAN_POINT('Ctrl Pts',(31.787966822558,-4.82876170189046,335.943832896979));
#65472=CARTESIAN_POINT('Ctrl Pts',(31.7802760210701,-4.80073416488714,336.077364990455));
#65473=CARTESIAN_POINT('Ctrl Pts',(31.7725852195822,-4.76721263948652,336.209490269667));
#65474=CARTESIAN_POINT('Ctrl Pts',(31.7648938427455,-4.73368860634084,336.341625433171));
#65475=CARTESIAN_POINT('Ctrl Pts',(31.7572024659088,-4.69466986486908,336.472353188198));
#65476=CARTESIAN_POINT('Ctrl Pts',(31.7495110890721,-4.65030996766537,336.60118714307));
#65477=CARTESIAN_POINT('Ctrl Pts',(31.7418174123076,-4.60593680566352,336.730059622747));
#65478=CARTESIAN_POINT('Ctrl Pts',(31.7341237355431,-4.55621944013669,336.857036800591));
#65479=CARTESIAN_POINT('Ctrl Pts',(31.7264300587786,-4.50136012885213,336.981650840305));
#65480=CARTESIAN_POINT('Ctrl Pts',(31.7187278898555,-4.44644026472813,337.106402427023));
#65481=CARTESIAN_POINT('Ctrl Pts',(31.7110257209323,-4.38636728307101,337.228785304049));
#65482=CARTESIAN_POINT('Ctrl Pts',(31.7033235520092,-4.3213902894302,337.348354536461));
#65483=CARTESIAN_POINT('Ctrl Pts',(31.6956166515253,-4.25637337942362,337.46799722209));
#65484=CARTESIAN_POINT('Ctrl Pts',(31.6879097510415,-4.1864466617007,337.584822481246));
#65485=CARTESIAN_POINT('Ctrl Pts',(31.6802028505576,-4.11190277012035,337.698414103057));
#65486=CARTESIAN_POINT('Ctrl Pts',(31.672484341483,-4.03724659610824,337.812176823308));
#65487=CARTESIAN_POINT('Ctrl Pts',(31.6647658324084,-3.95795959260941,337.922695859222));
#65488=CARTESIAN_POINT('Ctrl Pts',(31.6570473233338,-3.87437518747252,338.029587425574));
#65489=CARTESIAN_POINT('Ctrl Pts',(31.6527921799842,-3.82829587057259,338.088515766953));
#65490=CARTESIAN_POINT('Ctrl Pts',(31.6485370366347,-3.78091115388401,338.146342273655));
#65491=CARTESIAN_POINT('Ctrl Pts',(31.6442818932852,-3.73228155061267,338.203007569372));
#65492=CARTESIAN_POINT('Ctrl Pts',(31.6365068145068,-3.64342461552501,338.30654747438));
#65493=CARTESIAN_POINT('Ctrl Pts',(31.6287317357283,-3.5501154423416,338.406550624546));
#65494=CARTESIAN_POINT('Ctrl Pts',(31.6209566569499,-3.45266639300717,338.50261014689));
#65495=CARTESIAN_POINT('Ctrl Pts',(31.6131911459009,-3.35533726093187,338.598551461877));
#65496=CARTESIAN_POINT('Ctrl Pts',(31.6054256348519,-3.25387866476962,338.690558533115));
#65497=CARTESIAN_POINT('Ctrl Pts',(31.5976601238029,-3.14864322042121,338.778257393693));
#65498=CARTESIAN_POINT('Ctrl Pts',(31.5899023122807,-3.04351211732204,338.865869300595));
#65499=CARTESIAN_POINT('Ctrl Pts',(31.5821445007585,-2.93461191665274,338.949181248944));
#65500=CARTESIAN_POINT('Ctrl Pts',(31.5743866892363,-2.82233183113247,339.027856265742));
#65501=CARTESIAN_POINT('Ctrl Pts',(31.5666347157133,-2.71013623993746,339.106472077094));
#65502=CARTESIAN_POINT('Ctrl Pts',(31.5588827421903,-2.59456614536722,339.180457679052));
#65503=CARTESIAN_POINT('Ctrl Pts',(31.5511307686673,-2.47604328148428,339.249516764376));
#65504=CARTESIAN_POINT('Ctrl Pts',(31.5433820781096,-2.3575706121044,339.318546603138));
#65505=CARTESIAN_POINT('Ctrl Pts',(31.535633387552,-2.23614799759166,339.382653878562));
#65506=CARTESIAN_POINT('Ctrl Pts',(31.5278846969944,-2.11222536994269,339.4415860961));
#65507=CARTESIAN_POINT('Ctrl Pts',(31.5201376186166,-1.98832852543143,339.500506052298));
#65508=CARTESIAN_POINT('Ctrl Pts',(31.5123905402387,-1.86193305516648,339.554252924508));
#65509=CARTESIAN_POINT('Ctrl Pts',(31.5046434618609,-1.73351230438936,339.602620791791));
#65510=CARTESIAN_POINT('Ctrl Pts',(31.4968963185551,-1.60509047732282,339.650989064444));
#65511=CARTESIAN_POINT('Ctrl Pts',(31.4891491752493,-1.4746437016785,339.693978104481));
#65512=CARTESIAN_POINT('Ctrl Pts',(31.4814020319435,-1.3426636796606,339.731430788442));
#65513=CARTESIAN_POINT('Ctrl Pts',(31.4736531469154,-1.21065398573155,339.768891892562));
#65514=CARTESIAN_POINT('Ctrl Pts',(31.4659042618874,-1.07711073545531,339.800814057125));
#65515=CARTESIAN_POINT('Ctrl Pts',(31.4581553768593,-0.942538719708399,
339.827090616961));
#65516=CARTESIAN_POINT('Ctrl Pts',(31.4503982670845,-0.807823867833764,
339.853395067009));
#65517=CARTESIAN_POINT('Ctrl Pts',(31.4426411573098,-0.672078453466667,
339.874041867117));
#65518=CARTESIAN_POINT('Ctrl Pts',(31.434884047535,-0.53581589397678,339.888975801767));
#65519=CARTESIAN_POINT('Ctrl Pts',(31.4271227926089,-0.399480520131655,
339.903917716634));
#65520=CARTESIAN_POINT('Ctrl Pts',(31.4193615376827,-0.262627840311631,
339.913140656849));
#65521=CARTESIAN_POINT('Ctrl Pts',(31.4116002827565,-0.125773254256806,
339.916641552016));
#65522=CARTESIAN_POINT('Ctrl Pts',(31.4038266123519,0.011300254534714,339.920148047475));
#65523=CARTESIAN_POINT('Ctrl Pts',(31.3960529419472,0.148375284626583,339.917914213039));
#65524=CARTESIAN_POINT('Ctrl Pts',(31.3882792715425,0.28493868404132,339.909989104757));
#65525=CARTESIAN_POINT('Ctrl Pts',(31.3808674673655,0.415145024357676,339.902432912173));
#65526=CARTESIAN_POINT('Ctrl Pts',(31.3734556631884,0.544886008445155,339.889703407325));
#65527=CARTESIAN_POINT('Ctrl Pts',(31.3660438590113,0.673725692947513,339.871886364968));
#65528=CARTESIAN_POINT('Ctrl Pts',(31.3582687802329,0.808880194181423,339.853196056291));
#65529=CARTESIAN_POINT('Ctrl Pts',(31.3504937014545,0.943469924318875,339.828847824632));
#65530=CARTESIAN_POINT('Ctrl Pts',(31.3427186226761,1.07698369821825,339.798884159497));
#65531=CARTESIAN_POINT('Ctrl Pts',(31.3349531116271,1.21033317491894,339.76895736656));
#65532=CARTESIAN_POINT('Ctrl Pts',(31.3271876005781,1.34260895208501,339.733428974134));
#65533=CARTESIAN_POINT('Ctrl Pts',(31.319422089529,1.47330573226343,339.6923931295));
#65534=CARTESIAN_POINT('Ctrl Pts',(31.3116642780068,1.60387292620369,339.651397972025));
#65535=CARTESIAN_POINT('Ctrl Pts',(31.3039064664846,1.73286386822704,339.604906345689));
#65536=CARTESIAN_POINT('Ctrl Pts',(31.2961486549624,1.85978456521492,339.553063192345));
#65537=CARTESIAN_POINT('Ctrl Pts',(31.2883966814394,1.98660975035308,339.501259052619));
#65538=CARTESIAN_POINT('Ctrl Pts',(31.2806447079164,2.11136743103507,339.444111549027));
#65539=CARTESIAN_POINT('Ctrl Pts',(31.2728927343935,2.23358021168292,339.381814977892));
#65540=CARTESIAN_POINT('Ctrl Pts',(31.2651440438358,2.35574123514595,339.319544789392));
#65541=CARTESIAN_POINT('Ctrl Pts',(31.2573953532782,2.47535915466006,339.252130047617));
#65542=CARTESIAN_POINT('Ctrl Pts',(31.2496466627206,2.5919781581514,339.179812470694));
#65543=CARTESIAN_POINT('Ctrl Pts',(31.2418995843427,2.70857289808504,339.107509940046));
#65544=CARTESIAN_POINT('Ctrl Pts',(31.2341525059649,2.82216963109671,339.030306809119));
#65545=CARTESIAN_POINT('Ctrl Pts',(31.2264054275871,2.93233903960476,338.948489688388));
#65546=CARTESIAN_POINT('Ctrl Pts',(31.2186582842812,3.04250937143871,338.866671881952));
#65547=CARTESIAN_POINT('Ctrl Pts',(31.2109111409754,3.14925200767299,338.780240241627));
#65548=CARTESIAN_POINT('Ctrl Pts',(31.2031639976696,3.25216873156023,338.689523221768));
#65549=CARTESIAN_POINT('Ctrl Pts',(31.1954151126415,3.35510859331142,338.598785806797));
#65550=CARTESIAN_POINT('Ctrl Pts',(31.1876662276135,3.45422053795569,338.503761353558));
#65551=CARTESIAN_POINT('Ctrl Pts',(31.1799173425854,3.54914169716858,338.404816628824));
#65552=CARTESIAN_POINT('Ctrl Pts',(31.1721602328107,3.64416360668084,338.305766883138));
#65553=CARTESIAN_POINT('Ctrl Pts',(31.1644031230359,3.73498557415616,338.202788836447));
#65554=CARTESIAN_POINT('Ctrl Pts',(31.1566460132612,3.82128332808883,338.096284352086));
#65555=CARTESIAN_POINT('Ctrl Pts',(31.1488847583351,3.90762719678175,337.989722955134));
#65556=CARTESIAN_POINT('Ctrl Pts',(31.1411235034089,3.98944180162696,337.879631679212));
#65557=CARTESIAN_POINT('Ctrl Pts',(31.1333622484828,4.06644564828986,337.766442273391));
#65558=CARTESIAN_POINT('Ctrl Pts',(31.1255885780781,4.14357267601213,337.653071801408));
#65559=CARTESIAN_POINT('Ctrl Pts',(31.1178149076735,4.21587336112481,337.536593628246));
#65560=CARTESIAN_POINT('Ctrl Pts',(31.1100412372688,4.28311125992551,337.417465821392));
#65561=CARTESIAN_POINT('Ctrl Pts',(31.1026294330916,4.34721921836145,337.303883442606));
#65562=CARTESIAN_POINT('Ctrl Pts',(31.0952176289144,4.40672499718929,337.18789281569));
#65563=CARTESIAN_POINT('Ctrl Pts',(31.0878058247372,4.46146481226643,337.069906952355));
#65564=CARTESIAN_POINT('Ctrl Pts',(31.0800307459588,4.5188875887413,336.946138250398));
#65565=CARTESIAN_POINT('Ctrl Pts',(31.0722556671803,4.57124686702669,336.819782649727));
#65566=CARTESIAN_POINT('Ctrl Pts',(31.0644805884019,4.61830174584348,336.691293010344));
#65567=CARTESIAN_POINT('Ctrl Pts',(31.0567150773529,4.66529872063617,336.562961485643));
#65568=CARTESIAN_POINT('Ctrl Pts',(31.0489495663039,4.70700415048781,336.432501510884));
#65569=CARTESIAN_POINT('Ctrl Pts',(31.0411840552549,4.74322376040758,336.30038894997));
#65570=CARTESIAN_POINT('Ctrl Pts',(31.0334262437326,4.77940745847878,336.168407379045));
#65571=CARTESIAN_POINT('Ctrl Pts',(31.0256684322104,4.8101160582647,336.034776857297));
#65572=CARTESIAN_POINT('Ctrl Pts',(31.0179106206881,4.83520411644096,335.899991230431));
#65573=CARTESIAN_POINT('Ctrl Pts',(31.0101586471651,4.86027329505767,335.765307034024));
#65574=CARTESIAN_POINT('Ctrl Pts',(31.0024066736422,4.87973027970994,335.629469845434));
#65575=CARTESIAN_POINT('Ctrl Pts',(30.9946547001192,4.89348011217991,335.492986261674));
#65576=CARTESIAN_POINT('Ctrl Pts',(30.9869060095615,4.90722412158774,335.356560478793));
#65577=CARTESIAN_POINT('Ctrl Pts',(30.9791573190039,4.9152657469226,335.219489233305));
#65578=CARTESIAN_POINT('Ctrl Pts',(30.9714086284463,4.91756158804584,335.082286634857));
#65579=CARTESIAN_POINT('Ctrl Pts',(30.9636615500684,4.91985695150017,334.945112582555));
#65580=CARTESIAN_POINT('Ctrl Pts',(30.9559144716906,4.91640890205861,334.807807622225));
#65581=CARTESIAN_POINT('Ctrl Pts',(30.9481673933127,4.90722612820735,334.670887877557));
#65582=CARTESIAN_POINT('Ctrl Pts',(30.9404202500069,4.89804327739564,334.533966985369));
#65583=CARTESIAN_POINT('Ctrl Pts',(30.9326731067011,4.88312563246593,334.39743170528));
#65584=CARTESIAN_POINT('Ctrl Pts',(30.9249259633953,4.86253389975909,334.261794651744));
#65585=CARTESIAN_POINT('Ctrl Pts',(30.9171770783672,4.84193753759356,334.126127104119));
#65586=CARTESIAN_POINT('Ctrl Pts',(30.9094281933391,4.81566460789602,333.991358571257));
#65587=CARTESIAN_POINT('Ctrl Pts',(30.901679308311,4.78382716379953,333.85799267542));
#65588=CARTESIAN_POINT('Ctrl Pts',(30.8939221985362,4.75195592711084,333.724485223643));
#65589=CARTESIAN_POINT('Ctrl Pts',(30.8861650887615,4.71450846867204,333.592383763648));
#65590=CARTESIAN_POINT('Ctrl Pts',(30.8784079789868,4.67164724201592,333.46217845357));
#65591=CARTESIAN_POINT('Ctrl Pts',(30.8706467240606,4.62876311169068,333.331903565937));
#65592=CARTESIAN_POINT('Ctrl Pts',(30.8628854691344,4.58045958627627,333.203527212847));
#65593=CARTESIAN_POINT('Ctrl Pts',(30.8551242142082,4.52694740003962,333.077519753086));
#65594=CARTESIAN_POINT('Ctrl Pts',(30.8473505438035,4.47334961174464,332.951310722455));
#65595=CARTESIAN_POINT('Ctrl Pts',(30.8395768733989,4.41452668030623,332.827478510862));
#65596=CARTESIAN_POINT('Ctrl Pts',(30.8318032029942,4.35073585119288,332.706469835462));
#65597=CARTESIAN_POINT('Ctrl Pts',(30.8243913988173,4.28991450052324,332.591094143017));
#65598=CARTESIAN_POINT('Ctrl Pts',(30.8169795946403,4.22457749916489,332.47828528034));
#65599=CARTESIAN_POINT('Ctrl Pts',(30.8095677904634,4.15498352447909,332.368404481345));
#65600=CARTESIAN_POINT('Ctrl Pts',(30.8017927116849,4.08197854178278,332.25313809707));
#65601=CARTESIAN_POINT('Ctrl Pts',(30.7940176329065,4.00405803135536,332.140729797118));
#65602=CARTESIAN_POINT('Ctrl Pts',(30.7862425541281,3.92147244732838,332.031627229045));
#65603=CARTESIAN_POINT('Ctrl Pts',(30.7784770430791,3.83898849012032,331.922658918629));
#65604=CARTESIAN_POINT('Ctrl Pts',(30.7707115320301,3.75185111525413,331.816988554787));
#65605=CARTESIAN_POINT('Ctrl Pts',(30.7629460209811,3.66035535349278,331.715037024766));
#65606=CARTESIAN_POINT('Ctrl Pts',(30.7551882094589,3.56895031004566,331.613186579985));
#65607=CARTESIAN_POINT('Ctrl Pts',(30.7474303979367,3.47319573882904,331.51504792025));
#65608=CARTESIAN_POINT('Ctrl Pts',(30.7396725864145,3.37342821750476,331.421010600205));
#65609=CARTESIAN_POINT('Ctrl Pts',(30.7319206128915,3.27373577440354,331.327044046225));
#65610=CARTESIAN_POINT('Ctrl Pts',(30.7241686393685,3.17003667539488,331.237172955651));
#65611=CARTESIAN_POINT('Ctrl Pts',(30.7164166658455,3.06270554137598,331.151751329588));
#65612=CARTESIAN_POINT('Ctrl Pts',(30.7086679752878,2.95541986215649,331.066365879635));
#65613=CARTESIAN_POINT('Ctrl Pts',(30.7009192847302,2.84450551243674,330.985426389251));
#65614=CARTESIAN_POINT('Ctrl Pts',(30.6931705941726,2.73037133167992,330.909247568767));
#65615=CARTESIAN_POINT('Ctrl Pts',(30.6854235157948,2.61626089749268,330.833084597923));
#65616=CARTESIAN_POINT('Ctrl Pts',(30.677676437417,2.49893228967761,330.761680543668));
#65617=CARTESIAN_POINT('Ctrl Pts',(30.6699293590392,2.37882422949319,330.695307403812));
#65618=CARTESIAN_POINT('Ctrl Pts',(30.6621822157334,2.25871516268753,330.628933707685));
#65619=CARTESIAN_POINT('Ctrl Pts',(30.6544350724276,2.1358269391622,330.567591199111));
#65620=CARTESIAN_POINT('Ctrl Pts',(30.6466879291218,2.01062347903329,330.511506233929));
#65621=CARTESIAN_POINT('Ctrl Pts',(30.6389390440937,1.88539187050874,330.455408659656));
#65622=CARTESIAN_POINT('Ctrl Pts',(30.6311901590656,1.75784434626526,330.404571140598));
#65623=CARTESIAN_POINT('Ctrl Pts',(30.6234412740376,1.62846505138709,330.35917198779));
#65624=CARTESIAN_POINT('Ctrl Pts',(30.6156841642628,1.49894843198843,330.313724647852));
#65625=CARTESIAN_POINT('Ctrl Pts',(30.6079270544881,1.36759652752169,330.273727334576));
#65626=CARTESIAN_POINT('Ctrl Pts',(30.6001699447134,1.23490943534894,330.239308690013));
#65627=CARTESIAN_POINT('Ctrl Pts',(30.5924086897872,1.10215143943639,330.204871653227));
#65628=CARTESIAN_POINT('Ctrl Pts',(30.584647434861,0.968057216076455,330.176019307367));
#65629=CARTESIAN_POINT('Ctrl Pts',(30.5768861799348,0.833136340411268,330.152828979623));
#65630=CARTESIAN_POINT('Ctrl Pts',(30.5691125095302,0.69799963531581,330.129601554911));
#65631=CARTESIAN_POINT('Ctrl Pts',(30.5613388391255,0.562034023282853,330.112054297706));
#65632=CARTESIAN_POINT('Ctrl Pts',(30.5535651687209,0.425754368582244,330.10021262909));
#65633=CARTESIAN_POINT('Ctrl Pts',(30.5461533645437,0.295818564593465,330.088922192996));
#65634=CARTESIAN_POINT('Ctrl Pts',(30.5387415603666,0.16559758482116,330.082818122776));
#65635=CARTESIAN_POINT('Ctrl Pts',(30.5313297561895,0.0355351837341363,
330.081878375516));
#65636=CARTESIAN_POINT('Ctrl Pts',(30.523554677411,-0.10090196306498,330.080892568444));
#65637=CARTESIAN_POINT('Ctrl Pts',(30.5157795986325,-0.237595759891083,
330.085587006932));
#65638=CARTESIAN_POINT('Ctrl Pts',(30.508004519854,-0.374034235261797,330.095993326539));
#65639=CARTESIAN_POINT('Ctrl Pts',(30.500239008805,-0.510304814402098,330.106386840506));
#65640=CARTESIAN_POINT('Ctrl Pts',(30.492473497756,-0.646320311217115,330.122478220786));
#65641=CARTESIAN_POINT('Ctrl Pts',(30.484707986707,-0.781567134566584,330.144247135957));
#65642=CARTESIAN_POINT('Ctrl Pts',(30.4769501751849,-0.916679860296481,
330.165994467184));
#65643=CARTESIAN_POINT('Ctrl Pts',(30.4691923636627,-1.05102504584502,330.193408068977));
#65644=CARTESIAN_POINT('Ctrl Pts',(30.4614345521406,-1.18409296491653,330.226415716368));
#65645=CARTESIAN_POINT('Ctrl Pts',(30.4536825786176,-1.31706074615948,330.259398524459));
#65646=CARTESIAN_POINT('Ctrl Pts',(30.4459306050945,-1.44875279626469,330.297966905227));
#65647=CARTESIAN_POINT('Ctrl Pts',(30.4381786315715,-1.57866869928789,330.341997402278));
#65648=CARTESIAN_POINT('Ctrl Pts',(30.4304299410139,-1.7085295828492,330.386009252387));
#65649=CARTESIAN_POINT('Ctrl Pts',(30.4226812504563,-1.83661544597911,330.435478492766));
#65650=CARTESIAN_POINT('Ctrl Pts',(30.4149325598987,-1.96244039555348,330.490231629407));
#65651=CARTESIAN_POINT('Ctrl Pts',(30.4071854815209,-2.08823916619601,330.5449733742));
#65652=CARTESIAN_POINT('Ctrl Pts',(30.399438403143,-2.21177760076029,330.604996672687));
#65653=CARTESIAN_POINT('Ctrl Pts',(30.3916913247652,-2.33258955323889,330.670079788423));
#65654=CARTESIAN_POINT('Ctrl Pts',(30.3839441814594,-2.45340251823852,330.735163449619));
#65655=CARTESIAN_POINT('Ctrl Pts',(30.3761970381535,-2.57148861145812,330.805306827265));
#65656=CARTESIAN_POINT('Ctrl Pts',(30.3684498948476,-2.68640643164944,330.880242295172));
#65657=CARTESIAN_POINT('Ctrl Pts',(30.3607010098195,-2.80135008780619,330.955194610162));
#65658=CARTESIAN_POINT('Ctrl Pts',(30.3529521247915,-2.91312372619639,331.034940945788));
#65659=CARTESIAN_POINT('Ctrl Pts',(30.3452032397634,-3.02131540258246,331.11917066845));
#65660=CARTESIAN_POINT('Ctrl Pts',(30.3374461299887,-3.12962191473137,331.20348979341));
#65661=CARTESIAN_POINT('Ctrl Pts',(30.329689020214,-3.23433856124815,331.292301570887));
#65662=CARTESIAN_POINT('Ctrl Pts',(30.3219319104392,-3.3350865329092,331.385255073936));
#65663=CARTESIAN_POINT('Ctrl Pts',(30.3141706555131,-3.43588834106494,331.478258248364));
#65664=CARTESIAN_POINT('Ctrl Pts',(30.306409400587,-3.53271697282055,331.57540728167));
#65665=CARTESIAN_POINT('Ctrl Pts',(30.2986481456608,-3.6252316417453,331.676315507424));
#65666=CARTESIAN_POINT('Ctrl Pts',(30.2908744752562,-3.71789430399012,331.777385153454));
#65667=CARTESIAN_POINT('Ctrl Pts',(30.2831008048515,-3.80622896130463,331.882225709576));
#65668=CARTESIAN_POINT('Ctrl Pts',(30.2753271344468,-3.88993561395867,331.99041797225));
#65669=CARTESIAN_POINT('Ctrl Pts',(30.2679153302697,-3.96974570179313,332.093573859067));
#65670=CARTESIAN_POINT('Ctrl Pts',(30.2605035260926,-4.04534878889836,332.199776196451));
#65671=CARTESIAN_POINT('Ctrl Pts',(30.2530917219155,-4.1165232706243,332.308639893119));
#65672=CARTESIAN_POINT('Ctrl Pts',(30.2451556062878,-4.19273263925065,332.425204613904));
#65673=CARTESIAN_POINT('Ctrl Pts',(30.2372194906601,-4.26409775774852,332.545177455763));
#65674=CARTESIAN_POINT('Ctrl Pts',(30.2292833750324,-4.33030650368065,332.668127652147));
#65675=CARTESIAN_POINT('Ctrl Pts',(30.2213581817776,-4.39642412737518,332.790908633772));
#65676=CARTESIAN_POINT('Ctrl Pts',(30.2134329885229,-4.45739933324267,332.916658489957));
#65677=CARTESIAN_POINT('Ctrl Pts',(30.2055077952681,-4.51296290784668,333.044917174414));
#65678=CARTESIAN_POINT('Ctrl Pts',(30.1975920649108,-4.56846013802329,333.173022714496));
#65679=CARTESIAN_POINT('Ctrl Pts',(30.1896763345534,-4.61855845715624,333.303630781464));
#65680=CARTESIAN_POINT('Ctrl Pts',(30.1817606041961,-4.66303434688629,333.436256497293));
#65681=CARTESIAN_POINT('Ctrl Pts',(30.1738548472716,-4.70745419917215,333.568715111211));
#65682=CARTESIAN_POINT('Ctrl Pts',(30.1659490903471,-4.74626562370331,333.703185958915));
#65683=CARTESIAN_POINT('Ctrl Pts',(30.1580433334226,-4.77929323461932,333.839164421625));
#65684=CARTESIAN_POINT('Ctrl Pts',(30.1501434334114,-4.81229637730814,333.975042145837));
#65685=CARTESIAN_POINT('Ctrl Pts',(30.1422435334003,-4.8395241506503,334.112424903701));
#65686=CARTESIAN_POINT('Ctrl Pts',(30.1343436333892,-4.86085091019586,334.250792758078));
#65687=CARTESIAN_POINT('Ctrl Pts',(30.1264486619213,-4.88216436452783,334.38907428833));
#65688=CARTESIAN_POINT('Ctrl Pts',(30.1185536904535,-4.89758408313149,334.528339326433));
#65689=CARTESIAN_POINT('Ctrl Pts',(30.1106587189856,-4.90703550375296,334.668057795079));
#65690=CARTESIAN_POINT('Ctrl Pts',(30.1043782714933,-4.91455410609148,334.779203795999));
#65691=CARTESIAN_POINT('Ctrl Pts',(30.098097824001,-4.91829683194439,334.890636452684));
#65692=CARTESIAN_POINT('Ctrl Pts',(30.0918173765087,-4.91824955753956,335.002086207555));
#65693=CARTESIAN_POINT('',(28.3418173765442,-4.91824878394571,335.00345857146));
#65694=CARTESIAN_POINT('Ctrl Pts',(30.0918173764651,-4.91824955753923,335.002086208329));
#65695=CARTESIAN_POINT('Ctrl Pts',(30.0833748463321,-4.91818600860648,335.151903226139));
#65696=CARTESIAN_POINT('Ctrl Pts',(30.0749323161992,-4.91127285299927,335.301501189361));
#65697=CARTESIAN_POINT('Ctrl Pts',(30.0664897860662,-4.89759480406423,335.450275690775));
#65698=CARTESIAN_POINT('Ctrl Pts',(30.0580087662007,-4.88385439651897,335.59972845933));
#65699=CARTESIAN_POINT('Ctrl Pts',(30.0495277463351,-4.86328735742158,335.748349980473));
#65700=CARTESIAN_POINT('Ctrl Pts',(30.0410467264695,-4.83603008344163,335.895542346596));
#65701=CARTESIAN_POINT('Ctrl Pts',(30.0325460595063,-4.80870966536653,336.043075697985));
#65702=CARTESIAN_POINT('Ctrl Pts',(30.0240453925431,-4.77466809916791,336.18917301959));
#65703=CARTESIAN_POINT('Ctrl Pts',(30.0155447255798,-4.73409179891901,336.333250877332));
#65704=CARTESIAN_POINT('Ctrl Pts',(30.0070152556246,-4.69337801312253,336.477816917167));
#65705=CARTESIAN_POINT('Ctrl Pts',(29.9984857856693,-4.64608526133677,336.620349544757));
#65706=CARTESIAN_POINT('Ctrl Pts',(29.989956315714,-4.59244935944606,336.760281779552));
#65707=CARTESIAN_POINT('Ctrl Pts',(29.9849221063565,-4.56079271951306,336.842871690708));
#65708=CARTESIAN_POINT('Ctrl Pts',(29.9798878969991,-4.52692731909805,336.924556191571));
#65709=CARTESIAN_POINT('Ctrl Pts',(29.9748536876417,-4.4909090793162,337.005222856397));
#65710=CARTESIAN_POINT('Ctrl Pts',(29.9670786088632,-4.435280750838,337.129808392928));
#65711=CARTESIAN_POINT('Ctrl Pts',(29.9593035300848,-4.37437626530274,337.252274206464));
#65712=CARTESIAN_POINT('Ctrl Pts',(29.9515284513063,-4.30837893831905,337.372141223947));
#65713=CARTESIAN_POINT('Ctrl Pts',(29.9437629402573,-4.24246282524772,337.491860737434));
#65714=CARTESIAN_POINT('Ctrl Pts',(29.9359974292083,-4.17146652711353,337.608987478806));
#65715=CARTESIAN_POINT('Ctrl Pts',(29.9282319181593,-4.09562132785343,337.723062430671));
#65716=CARTESIAN_POINT('Ctrl Pts',(29.9204741066371,-4.01985132932916,337.83702427689));
#65717=CARTESIAN_POINT('Ctrl Pts',(29.9127162951148,-3.93924221229227,337.94794003183));
#65718=CARTESIAN_POINT('Ctrl Pts',(29.9049584835926,-3.85407088995616,338.055375695016));
#65719=CARTESIAN_POINT('Ctrl Pts',(29.8972065100696,-3.76896366174128,338.162730509457));
#65720=CARTESIAN_POINT('Ctrl Pts',(29.8894545365467,-3.67930130369825,338.266610139829));
#65721=CARTESIAN_POINT('Ctrl Pts',(29.8817025630237,-3.58540349963867,338.366610284437));
#65722=CARTESIAN_POINT('Ctrl Pts',(29.8739538724661,-3.49154546135472,338.466568078925));
#65723=CARTESIAN_POINT('Ctrl Pts',(29.8662051819084,-3.3934558116268,338.562649371036));
#65724=CARTESIAN_POINT('Ctrl Pts',(29.8584564913508,-3.29149375881297,338.654483807352));
#65725=CARTESIAN_POINT('Ctrl Pts',(29.850709412973,-3.18955292005598,338.746299136746));
#65726=CARTESIAN_POINT('Ctrl Pts',(29.8429623345951,-3.08374157103421,338.83386910645));
#65727=CARTESIAN_POINT('Ctrl Pts',(29.8352152562173,-2.97445464637312,338.916861322433));
#65728=CARTESIAN_POINT('Ctrl Pts',(29.8274681129115,-2.86516680578219,338.99985423397));
#65729=CARTESIAN_POINT('Ctrl Pts',(29.8197209696057,-2.75240364274228,339.07826907887));
#65730=CARTESIAN_POINT('Ctrl Pts',(29.8119738262999,-2.63659160635575,339.151814996335));
#65731=CARTESIAN_POINT('Ctrl Pts',(29.8042249412718,-2.52075353296469,339.225377448484));
#65732=CARTESIAN_POINT('Ctrl Pts',(29.7964760562436,-2.40186555215315,339.294068585491));
#65733=CARTESIAN_POINT('Ctrl Pts',(29.7887271712155,-2.280381051891,339.357642174465));
#65734=CARTESIAN_POINT('Ctrl Pts',(29.7809700614408,-2.1587676067251,339.421283241103));
#65735=CARTESIAN_POINT('Ctrl Pts',(29.7732129516661,-2.03455248366223,339.479795727625));
#65736=CARTESIAN_POINT('Ctrl Pts',(29.7654558418914,-1.90821201557302,339.532980252121));
#65737=CARTESIAN_POINT('Ctrl Pts',(29.7576945869652,-1.78180403517733,339.586193196727));
#65738=CARTESIAN_POINT('Ctrl Pts',(29.7499333320391,-1.65326881283957,339.634072369847));
#65739=CARTESIAN_POINT('Ctrl Pts',(29.7421720771129,-1.52309945667756,339.676467802473));
#65740=CARTESIAN_POINT('Ctrl Pts',(29.7343984067082,-1.39272187196779,339.718931053975));
#65741=CARTESIAN_POINT('Ctrl Pts',(29.7266247363035,-1.26070530632257,339.755892930093));
#65742=CARTESIAN_POINT('Ctrl Pts',(29.7188510658989,-1.12755558341491,339.787254063533));
#65743=CARTESIAN_POINT('Ctrl Pts',(29.7114392617218,-1.00060401214312,339.817155328665));
#65744=CARTESIAN_POINT('Ctrl Pts',(29.7040274575448,-0.872622688943411,
339.841965491052));
#65745=CARTESIAN_POINT('Ctrl Pts',(29.6966156533677,-0.744053911628984,
339.8616424014));
#65746=CARTESIAN_POINT('Ctrl Pts',(29.6888405745893,-0.609183595551083,
339.882283735738));
#65747=CARTESIAN_POINT('Ctrl Pts',(29.6810654958108,-0.473240568433122,
339.897341133303));
#65748=CARTESIAN_POINT('Ctrl Pts',(29.6732904170324,-0.336726895624577,
339.906709494179));
#65749=CARTESIAN_POINT('Ctrl Pts',(29.6655249059834,-0.200381211581309,
339.91606632669));
#65750=CARTESIAN_POINT('Ctrl Pts',(29.6577593949344,-0.0634666652849358,
339.919748025437));
#65751=CARTESIAN_POINT('Ctrl Pts',(29.6499938838853,0.0735055847371469,
339.917700681367));
#65752=CARTESIAN_POINT('Ctrl Pts',(29.6422360723631,0.210342026374456,339.915655367244));
#65753=CARTESIAN_POINT('Ctrl Pts',(29.634478260841,0.347235669566546,339.90789232035));
#65754=CARTESIAN_POINT('Ctrl Pts',(29.6267204493188,0.483671700423804,339.894409540354));
#65755=CARTESIAN_POINT('Ctrl Pts',(29.6189684757958,0.620005058841578,339.880936906577));
#65756=CARTESIAN_POINT('Ctrl Pts',(29.6112165022727,0.75588110295841,339.861753145442));
#65757=CARTESIAN_POINT('Ctrl Pts',(29.6034645287496,0.890786847601078,339.836908295041));
#65758=CARTESIAN_POINT('Ctrl Pts',(29.595715838192,1.02563545958043,339.812073966449));
#65759=CARTESIAN_POINT('Ctrl Pts',(29.5879671476344,1.15951420577163,339.781583387647));
#65760=CARTESIAN_POINT('Ctrl Pts',(29.5802184570768,1.29191725983002,339.74553820512));
#65761=CARTESIAN_POINT('Ctrl Pts',(29.5724713786989,1.42429276632716,339.709500522094));
#65762=CARTESIAN_POINT('Ctrl Pts',(29.5647243003211,1.55519281448465,339.667910636687));
#65763=CARTESIAN_POINT('Ctrl Pts',(29.5569772219433,1.68412416528252,339.620920780365));
#65764=CARTESIAN_POINT('Ctrl Pts',(29.5492300786375,1.81305659664911,339.573930530224));
#65765=CARTESIAN_POINT('Ctrl Pts',(29.5414829353317,1.94001993050217,339.521540352745));
#65766=CARTESIAN_POINT('Ctrl Pts',(29.5337357920259,2.06453879971386,339.463951456611));
#65767=CARTESIAN_POINT('Ctrl Pts',(29.5259869069978,2.18908566341097,339.40634961327));
#65768=CARTESIAN_POINT('Ctrl Pts',(29.5182380219697,2.31118661418876,339.343546889572));
#65769=CARTESIAN_POINT('Ctrl Pts',(29.5104891369416,2.43038923531106,339.27579129839));
#65770=CARTESIAN_POINT('Ctrl Pts',(29.5027320271669,2.54971837932717,339.207963790722));
#65771=CARTESIAN_POINT('Ctrl Pts',(29.4949749173921,2.66614270810379,339.135173107628));
#65772=CARTESIAN_POINT('Ctrl Pts',(29.4872178076174,2.77923678609253,339.057711910588));
#65773=CARTESIAN_POINT('Ctrl Pts',(29.4794565526912,2.89239129794042,338.980209320762));
#65774=CARTESIAN_POINT('Ctrl Pts',(29.4716952977651,3.00221170023099,338.898031478001));
#65775=CARTESIAN_POINT('Ctrl Pts',(29.463934042839,3.10830503172824,338.811511890606));
#65776=CARTESIAN_POINT('Ctrl Pts',(29.4561603724343,3.21456807798016,338.724853900068));
#65777=CARTESIAN_POINT('Ctrl Pts',(29.4483867020296,3.31709184693499,338.633840545607));
#65778=CARTESIAN_POINT('Ctrl Pts',(29.4406130316249,3.41551904829943,338.538843411795));
#65779=CARTESIAN_POINT('Ctrl Pts',(29.4332012274478,3.50936443976054,338.448268417416));
#65780=CARTESIAN_POINT('Ctrl Pts',(29.4257894232707,3.59948587216437,338.354072394849));
#65781=CARTESIAN_POINT('Ctrl Pts',(29.4183776190936,3.68560854854448,338.25660447236));
#65782=CARTESIAN_POINT('Ctrl Pts',(29.4106025403151,3.77595235383988,338.154359356648));
#65783=CARTESIAN_POINT('Ctrl Pts',(29.4028274615367,3.86218101307005,338.048190386743));
#65784=CARTESIAN_POINT('Ctrl Pts',(29.3950523827583,3.94393444910542,337.938462884513));
#65785=CARTESIAN_POINT('Ctrl Pts',(29.3872868717093,4.02558728233306,337.82887040896));
#65786=CARTESIAN_POINT('Ctrl Pts',(29.3795213606602,4.10277561851078,337.715728424483));
#65787=CARTESIAN_POINT('Ctrl Pts',(29.3717558496112,4.17517750715662,337.599437601912));
#65788=CARTESIAN_POINT('Ctrl Pts',(29.363998038089,4.24750760911913,337.483262082029));
#65789=CARTESIAN_POINT('Ctrl Pts',(29.3562402265668,4.31506050265605,337.363944266854));
#65790=CARTESIAN_POINT('Ctrl Pts',(29.3484824150446,4.37755591030942,337.241915991873));
#65791=CARTESIAN_POINT('Ctrl Pts',(29.3407304415216,4.44000428818668,337.119979547039));
#65792=CARTESIAN_POINT('Ctrl Pts',(29.3329784679986,4.49740257821792,336.995337048839));
#65793=CARTESIAN_POINT('Ctrl Pts',(29.3252264944755,4.5495152527901,336.868446955932));
#65794=CARTESIAN_POINT('Ctrl Pts',(29.3174778039179,4.60160585761365,336.741610601054));
#65795=CARTESIAN_POINT('Ctrl Pts',(29.3097291133602,4.64841515093551,336.612528905465));
#65796=CARTESIAN_POINT('Ctrl Pts',(29.3019804228026,4.68975487779492,336.481682236075));
#65797=CARTESIAN_POINT('Ctrl Pts',(29.2942333444247,4.73108600357889,336.350862790426));
#65798=CARTESIAN_POINT('Ctrl Pts',(29.2864862660469,4.76694970875933,336.218279473879));
#65799=CARTESIAN_POINT('Ctrl Pts',(29.2787391876691,4.79720708809017,336.08442944283));
#65800=CARTESIAN_POINT('Ctrl Pts',(29.2709920443633,4.82746472100695,335.95057828999));
#65801=CARTESIAN_POINT('Ctrl Pts',(29.2632449010575,4.85211584817201,335.815460782727));
#65802=CARTESIAN_POINT('Ctrl Pts',(29.2554977577516,4.87107242182887,335.679585552965));
#65803=CARTESIAN_POINT('Ctrl Pts',(29.2477488727235,4.89003325732592,335.543679775566));
#65804=CARTESIAN_POINT('Ctrl Pts',(29.2399999876955,4.90329693774831,335.407016323735));
#65805=CARTESIAN_POINT('Ctrl Pts',(29.2322511026674,4.91082719375468,335.270109858353));
#65806=CARTESIAN_POINT('Ctrl Pts',(29.2244939928926,4.91836544245259,335.133058079034));
#65807=CARTESIAN_POINT('Ctrl Pts',(29.2167368831179,4.92015808884482,334.99576316181));
#65808=CARTESIAN_POINT('Ctrl Pts',(29.2089797733431,4.91622101062853,334.858741240432));
#65809=CARTESIAN_POINT('Ctrl Pts',(29.201218518417,4.91228182856354,334.721646098921));
#65810=CARTESIAN_POINT('Ctrl Pts',(29.1934572634908,4.90260684857121,334.584824633638));
#65811=CARTESIAN_POINT('Ctrl Pts',(29.1856960085646,4.88726387102354,334.448787774548));
#65812=CARTESIAN_POINT('Ctrl Pts',(29.1779223381599,4.87189634971204,334.312533300817));
#65813=CARTESIAN_POINT('Ctrl Pts',(29.1701486677553,4.85084277245481,334.17706632781));
#65814=CARTESIAN_POINT('Ctrl Pts',(29.1623749973506,4.8242222623668,334.04288839429));
#65815=CARTESIAN_POINT('Ctrl Pts',(29.1549631931737,4.79884094342834,333.914956475859));
#65816=CARTESIAN_POINT('Ctrl Pts',(29.1475513889967,4.76839937670889,333.788196567919));
#65817=CARTESIAN_POINT('Ctrl Pts',(29.1401395848197,4.73304244320891,333.66302868644));
#65818=CARTESIAN_POINT('Ctrl Pts',(29.1323645060413,4.69595256107468,333.531725954231));
#65819=CARTESIAN_POINT('Ctrl Pts',(29.1245894272628,4.65333608457454,333.401760313487));
#65820=CARTESIAN_POINT('Ctrl Pts',(29.1168143484844,4.60530536226591,333.273632257372));
#65821=CARTESIAN_POINT('Ctrl Pts',(29.1090488374354,4.55733374481887,333.145661870988));
#65822=CARTESIAN_POINT('Ctrl Pts',(29.1012833263864,4.50396127406574,333.019524932469));
#65823=CARTESIAN_POINT('Ctrl Pts',(29.0935178153374,4.44535065677531,332.895709002821));
#65824=CARTESIAN_POINT('Ctrl Pts',(29.0857600038152,4.3867981520826,332.772015837028));
#65825=CARTESIAN_POINT('Ctrl Pts',(29.0780021922929,4.32301800264464,332.650639451429));
#65826=CARTESIAN_POINT('Ctrl Pts',(29.0702443807708,4.25422167392141,332.532049228279));
#65827=CARTESIAN_POINT('Ctrl Pts',(29.0624924072478,4.1854771166172,332.413548248033));
#65828=CARTESIAN_POINT('Ctrl Pts',(29.0547404337248,4.11172408899903,332.297829593646));
#65829=CARTESIAN_POINT('Ctrl Pts',(29.0469884602018,4.03322066122813,332.1853394236));
#65830=CARTESIAN_POINT('Ctrl Pts',(29.0392397696442,3.95475047970551,332.072896893207));
#65831=CARTESIAN_POINT('Ctrl Pts',(29.0314910790866,3.87153412258074,331.963680447631));
#65832=CARTESIAN_POINT('Ctrl Pts',(29.023742388529,3.78387366507585,331.858108348583));
#65833=CARTESIAN_POINT('Ctrl Pts',(29.0159953101512,3.69623144606129,331.752558214692));
#65834=CARTESIAN_POINT('Ctrl Pts',(29.0082482317734,3.60414721536821,331.650651219674));
#65835=CARTESIAN_POINT('Ctrl Pts',(29.0005011533955,3.50796387281852,331.552773211769));
#65836=CARTESIAN_POINT('Ctrl Pts',(28.9927540100897,3.41177972415979,331.454894383551));
#65837=CARTESIAN_POINT('Ctrl Pts',(28.9850068667839,3.31149666908763,331.361044888588));
#65838=CARTESIAN_POINT('Ctrl Pts',(28.9772597234781,3.20749477934344,331.271574018036));
#65839=CARTESIAN_POINT('Ctrl Pts',(28.96951083845,3.10346950776641,331.182083032532));
#65840=CARTESIAN_POINT('Ctrl Pts',(28.9617619534219,2.99572403408152,331.096972885164));
#65841=CARTESIAN_POINT('Ctrl Pts',(28.9540130683938,2.88467152018146,331.016552588127));
#65842=CARTESIAN_POINT('Ctrl Pts',(28.9462559586191,2.77350113399575,330.936046932157));
#65843=CARTESIAN_POINT('Ctrl Pts',(28.9384988488444,2.65901701286916,330.860241299871));
#65844=CARTESIAN_POINT('Ctrl Pts',(28.9307417390696,2.54166177701609,330.789401648963));
#65845=CARTESIAN_POINT('Ctrl Pts',(28.9229804841435,2.42424383027719,330.718524143611));
#65846=CARTESIAN_POINT('Ctrl Pts',(28.9152192292173,2.30395205433861,330.652618095014));
#65847=CARTESIAN_POINT('Ctrl Pts',(28.9074579742911,2.1812527917797,330.591902981915));
#65848=CARTESIAN_POINT('Ctrl Pts',(28.8996843038865,2.05835725038846,330.531090744421));
#65849=CARTESIAN_POINT('Ctrl Pts',(28.8919106334818,1.93304688401821,330.475486194508));
#65850=CARTESIAN_POINT('Ctrl Pts',(28.8841369630772,1.80580791166782,330.425260570409));
#65851=CARTESIAN_POINT('Ctrl Pts',(28.8767251589001,1.68449194409125,330.377372961194));
#65852=CARTESIAN_POINT('Ctrl Pts',(28.8693133547229,1.56142315470923,330.334374864422));
#65853=CARTESIAN_POINT('Ctrl Pts',(28.8619015505458,1.43703314733344,330.296371741308));
#65854=CARTESIAN_POINT('Ctrl Pts',(28.8541264717673,1.30654641515847,330.256505971925));
#65855=CARTESIAN_POINT('Ctrl Pts',(28.8463513929889,1.17419331439411,330.222011210563));
#65856=CARTESIAN_POINT('Ctrl Pts',(28.8385763142105,1.04045551867186,330.193063826494));
#65857=CARTESIAN_POINT('Ctrl Pts',(28.8308108031615,0.90688229582142,330.164152064023));
#65858=CARTESIAN_POINT('Ctrl Pts',(28.8230452921124,0.77192814677124,330.140774178162));
#65859=CARTESIAN_POINT('Ctrl Pts',(28.8152797810634,0.636091121940693,330.123057192555));
#65860=CARTESIAN_POINT('Ctrl Pts',(28.8075219695412,0.500388779915651,330.105357773391));
#65861=CARTESIAN_POINT('Ctrl Pts',(28.799764158019,0.363805689248478,330.09330813492));
#65862=CARTESIAN_POINT('Ctrl Pts',(28.7920063464968,0.226850999585688,330.086984460997));
#65863=CARTESIAN_POINT('Ctrl Pts',(28.7842543729738,0.0899993726701375,
330.080665545839));
#65864=CARTESIAN_POINT('Ctrl Pts',(28.7765023994509,-0.0472229077451133,
330.080064036391));
#65865=CARTESIAN_POINT('Ctrl Pts',(28.7687504259279,-0.184301000902406,
330.085204357904));
#65866=CARTESIAN_POINT('Ctrl Pts',(28.7610017353703,-0.321321041405862,
330.090342502488));
#65867=CARTESIAN_POINT('Ctrl Pts',(28.7532530448127,-0.458196626315287,
330.101217626997));
#65868=CARTESIAN_POINT('Ctrl Pts',(28.745504354255,-0.594412560198523,330.117802055347));
#65869=CARTESIAN_POINT('Ctrl Pts',(28.7377572758772,-0.730600153219017,
330.134383033167));
#65870=CARTESIAN_POINT('Ctrl Pts',(28.7300101974994,-0.866127980439663,
330.156670904861));
#65871=CARTESIAN_POINT('Ctrl Pts',(28.7222631191215,-1.00048601107593,330.184586123276));
#65872=CARTESIAN_POINT('Ctrl Pts',(28.7145159758157,-1.13484516776191,330.212501575648));
#65873=CARTESIAN_POINT('Ctrl Pts',(28.70676883251,-1.26803412560718,330.246044389296));
#65874=CARTESIAN_POINT('Ctrl Pts',(28.6990216892042,-1.39955347959971,330.285083975272));
#65875=CARTESIAN_POINT('Ctrl Pts',(28.6912728041761,-1.53110240193507,330.324132338175));
#65876=CARTESIAN_POINT('Ctrl Pts',(28.683523919148,-1.66098059884722,330.368679821285));
#65877=CARTESIAN_POINT('Ctrl Pts',(28.6757750341199,-1.78870462978005,330.418546212183));
#65878=CARTESIAN_POINT('Ctrl Pts',(28.6680179243452,-1.91656422831913,330.468465531783));
#65879=CARTESIAN_POINT('Ctrl Pts',(28.6602608145705,-2.04226472878972,330.523714894294));
#65880=CARTESIAN_POINT('Ctrl Pts',(28.6525037047958,-2.16534295449788,330.584066015903));
#65881=CARTESIAN_POINT('Ctrl Pts',(28.6447424498696,-2.28848694927466,330.644449387221));
#65882=CARTESIAN_POINT('Ctrl Pts',(28.6369811949434,-2.40900553388457,330.709939763336));
#65883=CARTESIAN_POINT('Ctrl Pts',(28.6292199400172,-2.52646177924276,330.780263759365));
#65884=CARTESIAN_POINT('Ctrl Pts',(28.6214462696126,-2.64410591631447,330.85070025087));
#65885=CARTESIAN_POINT('Ctrl Pts',(28.613672599208,-2.75867759815802,330.925985598783));
#65886=CARTESIAN_POINT('Ctrl Pts',(28.6058989288033,-2.86976970588929,331.005803598011));
#65887=CARTESIAN_POINT('Ctrl Pts',(28.5984871246262,-2.97569044927921,331.081906050173));
#65888=CARTESIAN_POINT('Ctrl Pts',(28.591075320449,-3.07844804979954,331.162128483327));
#65889=CARTESIAN_POINT('Ctrl Pts',(28.5836635162719,-3.17772025727494,331.246165023738));
#65890=CARTESIAN_POINT('Ctrl Pts',(28.5759987752936,-3.28038024915522,331.333069412949));
#65891=CARTESIAN_POINT('Ctrl Pts',(28.5683340343153,-3.37965706404458,331.424344666846));
#65892=CARTESIAN_POINT('Ctrl Pts',(28.560669293337,-3.47514759112905,331.519693651075));
#65893=CARTESIAN_POINT('Ctrl Pts',(28.5530140433566,-3.57051987542011,331.614924567777));
#65894=CARTESIAN_POINT('Ctrl Pts',(28.5453587933761,-3.66211491337428,331.714218901576));
#65895=CARTESIAN_POINT('Ctrl Pts',(28.5377035433956,-3.74956170951572,331.817238612614));
#65896=CARTESIAN_POINT('Ctrl Pts',(28.5300558174099,-3.83692255820402,331.920157070294));
#65897=CARTESIAN_POINT('Ctrl Pts',(28.5224080914242,-3.92014301570395,332.02679331707));
#65898=CARTESIAN_POINT('Ctrl Pts',(28.5147603654385,-3.99888847757235,332.136772100157));
#65899=CARTESIAN_POINT('Ctrl Pts',(28.507118327176,-4.07757537531465,332.246669090451));
#65900=CARTESIAN_POINT('Ctrl Pts',(28.4994762889135,-4.15179366607566,332.359903344221));
#65901=CARTESIAN_POINT('Ctrl Pts',(28.491834250651,-4.22124899208689,332.476066560048));
#65902=CARTESIAN_POINT('Ctrl Pts',(28.4841952106736,-4.29067706792492,332.592184200282));
#65903=CARTESIAN_POINT('Ctrl Pts',(28.4765561706961,-4.35534568807508,332.711228172525));
#65904=CARTESIAN_POINT('Ctrl Pts',(28.4689171307186,-4.41500402604019,332.832761546911));
#65905=CARTESIAN_POINT('Ctrl Pts',(28.4612793247114,-4.47465272711185,332.954275289436));
#65906=CARTESIAN_POINT('Ctrl Pts',(28.4536415187043,-4.52929257855681,333.078277272578));
#65907=CARTESIAN_POINT('Ctrl Pts',(28.4460037126971,-4.57871916181047,333.204306846989));
#65908=CARTESIAN_POINT('Ctrl Pts',(28.4383653776117,-4.62814916889134,333.330345151591));
#65909=CARTESIAN_POINT('Ctrl Pts',(28.4307270425263,-4.6723650439274,333.458410951158));
#65910=CARTESIAN_POINT('Ctrl Pts',(28.4230887074409,-4.7112110844228,333.588025077945));
#65911=CARTESIAN_POINT('Ctrl Pts',(28.415444459477,-4.75008719585863,333.717739539764));
#65912=CARTESIAN_POINT('Ctrl Pts',(28.407800211513,-4.7835850566836,333.849004335692));
#65913=CARTESIAN_POINT('Ctrl Pts',(28.4001559635491,-4.81159925285147,333.981326503506));
#65914=CARTESIAN_POINT('Ctrl Pts',(28.3925084442849,-4.83962543749063,334.113705297628));
#65915=CARTESIAN_POINT('Ctrl Pts',(28.3848609250207,-4.86216321672974,334.247141967853));
#65916=CARTESIAN_POINT('Ctrl Pts',(28.3772134057565,-4.87915880462597,334.381136184819));
#65917=CARTESIAN_POINT('Ctrl Pts',(28.3695564433058,-4.8961753787402,334.515295858364));
#65918=CARTESIAN_POINT('Ctrl Pts',(28.3618994808551,-4.90763606336808,334.65001405242));
#65919=CARTESIAN_POINT('Ctrl Pts',(28.3542425184044,-4.91353913253374,334.784787882405));
#65920=CARTESIAN_POINT('Ctrl Pts',(28.350100804451,-4.91673215118683,334.8576881553));
#65921=CARTESIAN_POINT('Ctrl Pts',(28.3459590904975,-4.9183000156394,334.930604730489));
#65922=CARTESIAN_POINT('Ctrl Pts',(28.3418173765441,-4.91824878394571,335.003458571461));
#65923=CARTESIAN_POINT('',(26.59181737648,-4.9182484316936,334.996072323401));
#65924=CARTESIAN_POINT('Ctrl Pts',(28.3418173765088,-4.91824878394527,335.003458572083));
#65925=CARTESIAN_POINT('Ctrl Pts',(28.3296867450051,-4.9180987318373,335.216839580139));
#65926=CARTESIAN_POINT('Ctrl Pts',(28.3175561135015,-4.90406196907175,335.429737823245));
#65927=CARTESIAN_POINT('Ctrl Pts',(28.3054254819979,-4.87632668485687,335.64079725737));
#65928=CARTESIAN_POINT('Ctrl Pts',(28.2976504032195,-4.85854986757834,335.776074940709));
#65929=CARTESIAN_POINT('Ctrl Pts',(28.2898753244411,-4.83511144100055,335.910826089138));
#65930=CARTESIAN_POINT('Ctrl Pts',(28.2821002456626,-4.8060504402412,336.044539242134));
#65931=CARTESIAN_POINT('Ctrl Pts',(28.2743347346136,-4.77702520089336,336.178087852582));
#65932=CARTESIAN_POINT('Ctrl Pts',(28.2665692235646,-4.74239123628207,336.310600630791));
#65933=CARTESIAN_POINT('Ctrl Pts',(28.2588037125156,-4.70223927789326,336.441571654805));
#65934=CARTESIAN_POINT('Ctrl Pts',(28.2510459009934,-4.66212713028812,336.572412820668));
#65935=CARTESIAN_POINT('Ctrl Pts',(28.2432880894712,-4.61650799054735,336.701714903145));
#65936=CARTESIAN_POINT('Ctrl Pts',(28.235530277949,-4.56552345994233,336.828982941204));
#65937=CARTESIAN_POINT('Ctrl Pts',(28.227778304426,-4.51457729681361,336.956155206029));
#65938=CARTESIAN_POINT('Ctrl Pts',(28.220026330903,-4.45827392429117,337.081296111805));
#65939=CARTESIAN_POINT('Ctrl Pts',(28.21227435738,-4.39680440911616,337.203926961239));
#65940=CARTESIAN_POINT('Ctrl Pts',(28.2045256668224,-4.33536092631716,337.326505876436));
#65941=CARTESIAN_POINT('Ctrl Pts',(28.1967769762649,-4.2687558271648,337.446576500838));
#65942=CARTESIAN_POINT('Ctrl Pts',(28.1890282857073,-4.19722774493399,337.563681399795));
#65943=CARTESIAN_POINT('Ctrl Pts',(28.1812812073295,-4.1257145447181,337.6807619341));
#65944=CARTESIAN_POINT('Ctrl Pts',(28.1735341289516,-4.04928060238351,337.794877636942));
#65945=CARTESIAN_POINT('Ctrl Pts',(28.1657870505738,-3.96820962151983,337.905597264278));
#65946=CARTESIAN_POINT('Ctrl Pts',(28.158039907268,-3.88713796120325,338.016317819551));
#65947=CARTESIAN_POINT('Ctrl Pts',(28.1502927639621,-3.80142941576291,338.123641927177));
#65948=CARTESIAN_POINT('Ctrl Pts',(28.1425456206563,-3.71140974181861,338.227169160554));
#65949=CARTESIAN_POINT('Ctrl Pts',(28.1347967356282,-3.62136982954056,338.330719669051));
#65950=CARTESIAN_POINT('Ctrl Pts',(28.1270478506002,-3.52701711651951,338.430471309791));
#65951=CARTESIAN_POINT('Ctrl Pts',(28.1192989655721,-3.4287159097258,338.526058744958));
#65952=CARTESIAN_POINT('Ctrl Pts',(28.1115418557974,-3.33031036501543,338.621747637616));
#65953=CARTESIAN_POINT('Ctrl Pts',(28.1037847460227,-3.227948235346,338.713263222551));
#65954=CARTESIAN_POINT('Ctrl Pts',(28.096027636248,-3.12202918419641,338.800278520783));
#65955=CARTESIAN_POINT('Ctrl Pts',(28.0882663813218,-3.01605353329245,338.887340317209));
#65956=CARTESIAN_POINT('Ctrl Pts',(28.0805051263956,-2.90651748556918,338.96989679999));
#65957=CARTESIAN_POINT('Ctrl Pts',(28.0727438714694,-2.7938508785489,339.047663564445));
#65958=CARTESIAN_POINT('Ctrl Pts',(28.0649702010648,-2.68100404167551,339.125554730378));
#65959=CARTESIAN_POINT('Ctrl Pts',(28.0571965306601,-2.56501696915984,339.198640658573));
#65960=CARTESIAN_POINT('Ctrl Pts',(28.0494228602555,-2.44634612069107,339.266681816152));
#65961=CARTESIAN_POINT('Ctrl Pts',(28.0420110560783,-2.33319942876795,339.331555641476));
#65962=CARTESIAN_POINT('Ctrl Pts',(28.0345992519012,-2.21761345267156,339.391843661645));
#65963=CARTESIAN_POINT('Ctrl Pts',(28.027187447724,-2.10000008820916,339.447379306066));
#65964=CARTESIAN_POINT('Ctrl Pts',(28.0194123689456,-1.9766221424033,339.505636917851));
#65965=CARTESIAN_POINT('Ctrl Pts',(28.0116372901671,-1.85062314938169,339.558848623339));
#65966=CARTESIAN_POINT('Ctrl Pts',(28.0038622113887,-1.72245433135183,339.606770467356));
#65967=CARTESIAN_POINT('Ctrl Pts',(27.9960967003397,-1.59444323321236,339.654633340494));
#65968=CARTESIAN_POINT('Ctrl Pts',(27.9883311892907,-1.46426798543332,339.697219168639));
#65969=CARTESIAN_POINT('Ctrl Pts',(27.9805656782417,-1.33240312859241,339.734330466435));
#65970=CARTESIAN_POINT('Ctrl Pts',(27.9728078667195,-1.20066901614088,339.771404968272));
#65971=CARTESIAN_POINT('Ctrl Pts',(27.9650500551973,-1.06724900230795,339.803015636602));
#65972=CARTESIAN_POINT('Ctrl Pts',(27.9572922436751,-0.932635938957153,
339.829013695142));
#65973=CARTESIAN_POINT('Ctrl Pts',(27.9495402701521,-0.798124176205531,
339.854992189317));
#65974=CARTESIAN_POINT('Ctrl Pts',(27.9417882966291,-0.662421533215169,
339.875366406883));
#65975=CARTESIAN_POINT('Ctrl Pts',(27.9340363231061,-0.526033953929984,
339.890037969363));
#65976=CARTESIAN_POINT('Ctrl Pts',(27.9262876325485,-0.389704134865414,
339.904703318428));
#65977=CARTESIAN_POINT('Ctrl Pts',(27.9185389419909,-0.252690344260004,
339.913670774108));
#65978=CARTESIAN_POINT('Ctrl Pts',(27.9107902514332,-0.115506386827868,
339.916893464079));
#65979=CARTESIAN_POINT('Ctrl Pts',(27.9030431730554,0.0216490283361404,
339.920115483542));
#65980=CARTESIAN_POINT('Ctrl Pts',(27.8952960946776,0.158974149383418,339.917595105551));
#65981=CARTESIAN_POINT('Ctrl Pts',(27.8875490162998,0.295952805707266,339.909337531612));
#65982=CARTESIAN_POINT('Ctrl Pts',(27.879801872994,0.432932610044187,339.901079888466));
#65983=CARTESIAN_POINT('Ctrl Pts',(27.8720547296881,0.569565553700036,339.887084976986));
#65984=CARTESIAN_POINT('Ctrl Pts',(27.8643075863823,0.705338623802703,339.867410039053));
#65985=CARTESIAN_POINT('Ctrl Pts',(27.8565587013542,0.841142218573888,339.847730677775));
#65986=CARTESIAN_POINT('Ctrl Pts',(27.8488098163261,0.976085168352783,339.822368805021));
#65987=CARTESIAN_POINT('Ctrl Pts',(27.841060931298,1.10966310537149,339.791433069039));
#65988=CARTESIAN_POINT('Ctrl Pts',(27.8333038215233,1.24338282339285,339.760464497546));
#65989=CARTESIAN_POINT('Ctrl Pts',(27.8255467117486,1.37573425306583,339.723910333078));
#65990=CARTESIAN_POINT('Ctrl Pts',(27.8177896019738,1.5062261499503,339.681929714093));
#65991=CARTESIAN_POINT('Ctrl Pts',(27.8100283470477,1.63678777753205,339.639926662007));
#65992=CARTESIAN_POINT('Ctrl Pts',(27.8022670921215,1.76548752576845,339.59249151255));
#65993=CARTESIAN_POINT('Ctrl Pts',(27.7945058371953,1.89185362294645,339.539831817573));
#65994=CARTESIAN_POINT('Ctrl Pts',(27.7867321667907,2.01842186469732,339.487087884245));
#65995=CARTESIAN_POINT('Ctrl Pts',(27.778958496386,2.14264864121181,339.429102869907));
#65996=CARTESIAN_POINT('Ctrl Pts',(27.7711848259813,2.26408550765253,339.366130996264));
#65997=CARTESIAN_POINT('Ctrl Pts',(27.7637730218042,2.37986945874392,339.30609047849));
#65998=CARTESIAN_POINT('Ctrl Pts',(27.7563612176272,2.49311714507877,339.241517072312));
#65999=CARTESIAN_POINT('Ctrl Pts',(27.7489494134502,2.60346559343578,339.172667008796));
#66000=CARTESIAN_POINT('Ctrl Pts',(27.7411743346717,2.71922254795856,339.100442398573));
#66001=CARTESIAN_POINT('Ctrl Pts',(27.7333992558933,2.83215469127028,339.023283064397));
#66002=CARTESIAN_POINT('Ctrl Pts',(27.7256241771148,2.94181269403341,338.941436430506));
#66003=CARTESIAN_POINT('Ctrl Pts',(27.7178586660658,3.05133575564297,338.859690514109));
#66004=CARTESIAN_POINT('Ctrl Pts',(27.7100931550168,3.15759238308679,338.773269006268));
#66005=CARTESIAN_POINT('Ctrl Pts',(27.7023276439678,3.26015970557934,338.682464087621));
#66006=CARTESIAN_POINT('Ctrl Pts',(27.6945698324456,3.36262533227309,338.591749202314));
#66007=CARTESIAN_POINT('Ctrl Pts',(27.6868120209233,3.46140864278015,338.496659812744));
#66008=CARTESIAN_POINT('Ctrl Pts',(27.6790542094011,3.55611781752552,338.397529857172));
#66009=CARTESIAN_POINT('Ctrl Pts',(27.6713022358781,3.65075572061336,338.298474500036));
#66010=CARTESIAN_POINT('Ctrl Pts',(27.663550262355,3.74132532156719,338.195384910653));
#66011=CARTESIAN_POINT('Ctrl Pts',(27.655798288832,3.82747009652994,338.088633309843));
#66012=CARTESIAN_POINT('Ctrl Pts',(27.6480495982744,3.91357838912935,337.981926918398));
#66013=CARTESIAN_POINT('Ctrl Pts',(27.6403009077167,3.99526533786943,337.871561903638));
#66014=CARTESIAN_POINT('Ctrl Pts',(27.6325522171591,4.07221347759927,337.757944969603));
#66015=CARTESIAN_POINT('Ctrl Pts',(27.6248051387812,4.14914560762594,337.64435167452));
#66016=CARTESIAN_POINT('Ctrl Pts',(27.6170580604034,4.22134067071622,337.527508129378));
#66017=CARTESIAN_POINT('Ctrl Pts',(27.6093109820256,4.2885237113934,337.407851207886));
#66018=CARTESIAN_POINT('Ctrl Pts',(27.6015638387197,4.35570731512909,337.288193283553));
#66019=CARTESIAN_POINT('Ctrl Pts',(27.593816695414,4.41787862130623,337.165722276667));
#66020=CARTESIAN_POINT('Ctrl Pts',(27.5860695521081,4.47480814514108,337.040900567563));
#66021=CARTESIAN_POINT('Ctrl Pts',(27.57832066708,4.53175046794154,336.916050795888));
#66022=CARTESIAN_POINT('Ctrl Pts',(27.5705717820519,4.58344850122072,336.788849625926));
#66023=CARTESIAN_POINT('Ctrl Pts',(27.5628228970238,4.62972066726931,336.659779987095));
#66024=CARTESIAN_POINT('Ctrl Pts',(27.5550657872491,4.6760419470731,336.530573352414));
#66025=CARTESIAN_POINT('Ctrl Pts',(27.5473086774744,4.71692572324246,336.399494655737));
#66026=CARTESIAN_POINT('Ctrl Pts',(27.5395515676996,4.75223997814796,336.267043113944));
#66027=CARTESIAN_POINT('Ctrl Pts',(27.5317903127734,4.78757310386213,336.134520794282));
#66028=CARTESIAN_POINT('Ctrl Pts',(27.5240290578473,4.8173306932602,336.000624549101));
#66029=CARTESIAN_POINT('Ctrl Pts',(27.5162678029211,4.84143197837612,335.865863419517));
#66030=CARTESIAN_POINT('Ctrl Pts',(27.5084941325164,4.86557181769364,335.730886716043));
#66031=CARTESIAN_POINT('Ctrl Pts',(27.5007204621117,4.88403721898356,335.595042750972));
#66032=CARTESIAN_POINT('Ctrl Pts',(27.4929467917071,4.8967992834685,335.458846205087));
#66033=CARTESIAN_POINT('Ctrl Pts',(27.48553498753,4.90896727078115,335.328989641181));
#66034=CARTESIAN_POINT('Ctrl Pts',(27.4781231833531,4.91595093713944,335.198812870405));
#66035=CARTESIAN_POINT('Ctrl Pts',(27.470711379176,4.91776932707573,335.068759786017));
#66036=CARTESIAN_POINT('Ctrl Pts',(27.4629363003976,4.91967684171952,334.932332412554));
#66037=CARTESIAN_POINT('Ctrl Pts',(27.4551612216192,4.91590597427971,334.795610020817));
#66038=CARTESIAN_POINT('Ctrl Pts',(27.4473861428407,4.90642163118969,334.659104356886));
#66039=CARTESIAN_POINT('Ctrl Pts',(27.4396206317917,4.89694895918766,334.522766671865));
#66040=CARTESIAN_POINT('Ctrl Pts',(27.4318551207428,4.881776827636,334.386645570204));
#66041=CARTESIAN_POINT('Ctrl Pts',(27.4240896096938,4.86092209781968,334.251254768677));
#66042=CARTESIAN_POINT('Ctrl Pts',(27.4163317981716,4.8400880455287,334.115998207525));
#66043=CARTESIAN_POINT('Ctrl Pts',(27.4085739866494,4.81358266669662,333.981470889346));
#66044=CARTESIAN_POINT('Ctrl Pts',(27.4008161751272,4.78147474107766,333.848183016736));
#66045=CARTESIAN_POINT('Ctrl Pts',(27.3930642016042,4.74939097769094,333.714995447476));
#66046=CARTESIAN_POINT('Ctrl Pts',(27.3853122280812,4.71171315061781,333.583045845723));
#66047=CARTESIAN_POINT('Ctrl Pts',(27.3775602545582,4.66856133276941,333.452835450034));
#66048=CARTESIAN_POINT('Ctrl Pts',(27.3698115640006,4.62542778974149,333.322680198526));
#66049=CARTESIAN_POINT('Ctrl Pts',(27.362062873443,4.57682498945489,333.194263058386));
#66050=CARTESIAN_POINT('Ctrl Pts',(27.3543141828854,4.52292313940507,333.068071083726));
#66051=CARTESIAN_POINT('Ctrl Pts',(27.3465671045076,4.46903250408535,332.941905364361));
#66052=CARTESIAN_POINT('Ctrl Pts',(27.3388200261297,4.40984516541813,332.817964248837));
#66053=CARTESIAN_POINT('Ctrl Pts',(27.3310729477519,4.34557970563935,332.696715370512));
#66054=CARTESIAN_POINT('Ctrl Pts',(27.3233258044461,4.28131370725411,332.575465476005));
#66055=CARTESIAN_POINT('Ctrl Pts',(27.3155786611403,4.21196968592095,332.456908209063));
#66056=CARTESIAN_POINT('Ctrl Pts',(27.3078315178345,4.13781227974334,332.341486768868));
#66057=CARTESIAN_POINT('Ctrl Pts',(27.3000826328064,4.06363820140642,332.226039379482));
#66058=CARTESIAN_POINT('Ctrl Pts',(27.2923337477783,3.98464879610733,332.1137295485));
#66059=CARTESIAN_POINT('Ctrl Pts',(27.2845848627502,3.90115190737911,332.004971309311));
#66060=CARTESIAN_POINT('Ctrl Pts',(27.2768277529754,3.81756639419051,331.896097633002));
#66061=CARTESIAN_POINT('Ctrl Pts',(27.2690706432008,3.72946407890935,331.790783389338));
#66062=CARTESIAN_POINT('Ctrl Pts',(27.261313533426,3.63719332134686,331.689409749659));
#66063=CARTESIAN_POINT('Ctrl Pts',(27.2535522784999,3.5448732572417,331.587981939149));
#66064=CARTESIAN_POINT('Ctrl Pts',(27.2457910235737,3.44838058723222,331.490499206142));
#66065=CARTESIAN_POINT('Ctrl Pts',(27.2380297686475,3.34809966666967,331.397304941499));
#66066=CARTESIAN_POINT('Ctrl Pts',(27.2302560982428,3.24765832931582,331.303961596405));
#66067=CARTESIAN_POINT('Ctrl Pts',(27.2224824278382,3.14341692916654,331.214920682293));
#66068=CARTESIAN_POINT('Ctrl Pts',(27.2147087574336,3.03579263348591,331.130485024067));
#66069=CARTESIAN_POINT('Ctrl Pts',(27.2072969532564,2.93317827466126,331.049979866044));
#66070=CARTESIAN_POINT('Ctrl Pts',(27.1998851490793,2.82748911350364,330.973661031803));
#66071=CARTESIAN_POINT('Ctrl Pts',(27.1924733449022,2.71910873541287,330.901752722504));
#66072=CARTESIAN_POINT('Ctrl Pts',(27.1846982661237,2.60541631214426,330.826319972763));
#66073=CARTESIAN_POINT('Ctrl Pts',(27.1769231873453,2.48840290334483,330.755502644344));
#66074=CARTESIAN_POINT('Ctrl Pts',(27.1691481085668,2.368479856067,330.689607183341));
#66075=CARTESIAN_POINT('Ctrl Pts',(27.1613825975178,2.24870438173336,330.623792810898));
#66076=CARTESIAN_POINT('Ctrl Pts',(27.1536170864689,2.12602673237098,330.562888441267));
#66077=CARTESIAN_POINT('Ctrl Pts',(27.1458515754198,2.00088802798299,330.507157897057));
#66078=CARTESIAN_POINT('Ctrl Pts',(27.1380937638976,1.87587339898483,330.451482609844));
#66079=CARTESIAN_POINT('Ctrl Pts',(27.1303359523754,1.74840292574922,330.400971097329));
#66080=CARTESIAN_POINT('Ctrl Pts',(27.1225781408532,1.61894286919439,330.355841621049));
#66081=CARTESIAN_POINT('Ctrl Pts',(27.1148261673302,1.4895802354377,330.31074610613));
#66082=CARTESIAN_POINT('Ctrl Pts',(27.1070741938072,1.35823136611897,330.271024693962));
#66083=CARTESIAN_POINT('Ctrl Pts',(27.0993222202842,1.22538274177925,330.236847661616));
#66084=CARTESIAN_POINT('Ctrl Pts',(27.0915735297266,1.09259037891063,330.202685103264));
#66085=CARTESIAN_POINT('Ctrl Pts',(27.083824839169,0.958299902044125,330.174062351817));
#66086=CARTESIAN_POINT('Ctrl Pts',(27.0760761486113,0.823012994415282,330.151099849087));
#66087=CARTESIAN_POINT('Ctrl Pts',(27.0683290702335,0.687754234357693,330.128142123898));
#66088=CARTESIAN_POINT('Ctrl Pts',(27.0605819918557,0.551499841024263,330.11084237034));
#66089=CARTESIAN_POINT('Ctrl Pts',(27.0528349134779,0.414761344671912,330.09926984119));
#66090=CARTESIAN_POINT('Ctrl Pts',(27.0450877701721,0.278021702319259,330.087697215052));
#66091=CARTESIAN_POINT('Ctrl Pts',(27.0373406268663,0.14079833833711,330.081851942024));
#66092=CARTESIAN_POINT('Ctrl Pts',(27.0295934835605,0.0036071592346469,
330.081751322788));
#66093=CARTESIAN_POINT('Ctrl Pts',(27.0218445985324,-0.13361486335753,330.081650680929));
#66094=CARTESIAN_POINT('Ctrl Pts',(27.0140957135042,-0.270804295873701,
330.087297263129));
#66095=CARTESIAN_POINT('Ctrl Pts',(27.0063468284761,-0.407446377004991,
330.098656254417));
#66096=CARTESIAN_POINT('Ctrl Pts',(26.9985897187014,-0.54423349145297,330.110027302255));
#66097=CARTESIAN_POINT('Ctrl Pts',(26.9908326089267,-0.680471703839216,
330.127122838579));
#66098=CARTESIAN_POINT('Ctrl Pts',(26.983075499152,-0.815651961568826,330.149856193875));
#66099=CARTESIAN_POINT('Ctrl Pts',(26.9753142442258,-0.950904455305848,
330.17260169715));
#66100=CARTESIAN_POINT('Ctrl Pts',(26.9675529892997,-1.0850974856846,330.200990941553));
#66101=CARTESIAN_POINT('Ctrl Pts',(26.9597917343736,-1.2177342912693,330.23488654297));
#66102=CARTESIAN_POINT('Ctrl Pts',(26.9520180639689,-1.3505832725167,330.268836366303));
#66103=CARTESIAN_POINT('Ctrl Pts',(26.9442443935642,-1.48187067978886,330.308310035788));
#66104=CARTESIAN_POINT('Ctrl Pts',(26.9364707231596,-1.61111610802111,330.353120622506));
#66105=CARTESIAN_POINT('Ctrl Pts',(26.9290589189825,-1.73434513047501,330.395845265632));
#66106=CARTESIAN_POINT('Ctrl Pts',(26.9216471148053,-1.85571773592336,330.443421035647));
#66107=CARTESIAN_POINT('Ctrl Pts',(26.9142353106282,-1.9748378087586,330.495646695518));
#66108=CARTESIAN_POINT('Ctrl Pts',(26.9064602318498,-2.09979631120362,330.550432090551));
#66109=CARTESIAN_POINT('Ctrl Pts',(26.8986851530714,-2.2226707832227,330.610507842477));
#66110=CARTESIAN_POINT('Ctrl Pts',(26.8909100742929,-2.34298092426293,330.67569387635));
#66111=CARTESIAN_POINT('Ctrl Pts',(26.8831445632439,-2.4631430160153,330.740799694658));
#66112=CARTESIAN_POINT('Ctrl Pts',(26.8753790521949,-2.58074671508766,330.81100309812));
#66113=CARTESIAN_POINT('Ctrl Pts',(26.8676135411459,-2.69533145207467,330.886075909067));
#66114=CARTESIAN_POINT('Ctrl Pts',(26.8598557296237,-2.80980257796128,330.961074285104));
#66115=CARTESIAN_POINT('Ctrl Pts',(26.8520979181015,-2.92126037377313,331.040932247739));
#66116=CARTESIAN_POINT('Ctrl Pts',(26.8443401065793,-3.0292689781907,331.125375822061));
#66117=CARTESIAN_POINT('Ctrl Pts',(26.8365881330563,-3.13719630270815,331.209755849915));
#66118=CARTESIAN_POINT('Ctrl Pts',(26.8288361595333,-3.24167929560479,331.298714380992));
#66119=CARTESIAN_POINT('Ctrl Pts',(26.8210841860103,-3.34231150472172,331.39193447012));
#66120=CARTESIAN_POINT('Ctrl Pts',(26.8133354954527,-3.44290109603848,331.485115080486));
#66121=CARTESIAN_POINT('Ctrl Pts',(26.8055868048951,-3.53964286098858,331.582553394263));
#66122=CARTESIAN_POINT('Ctrl Pts',(26.7978381143375,-3.63216402789683,331.683892713293));
#66123=CARTESIAN_POINT('Ctrl Pts',(26.7900910359596,-3.72466594500342,331.78521094783));
#66124=CARTESIAN_POINT('Ctrl Pts',(26.7823439575818,-3.81294874735247,331.890428284735));
#66125=CARTESIAN_POINT('Ctrl Pts',(26.774596879204,-3.89667738043269,331.999152043951));
#66126=CARTESIAN_POINT('Ctrl Pts',(26.7668497358982,-3.98040671523949,332.107876714377));
#66127=CARTESIAN_POINT('Ctrl Pts',(26.7591025925923,-4.0595815661577,332.220107556045));
#66128=CARTESIAN_POINT('Ctrl Pts',(26.7513554492865,-4.13390819806113,332.335420094555));
#66129=CARTESIAN_POINT('Ctrl Pts',(26.7436065642584,-4.20825154016942,332.450758557772));
#66130=CARTESIAN_POINT('Ctrl Pts',(26.7358576792304,-4.27774428259524,332.569179768012));
#66131=CARTESIAN_POINT('Ctrl Pts',(26.7281087942023,-4.34213713510919,332.690232011131));
#66132=CARTESIAN_POINT('Ctrl Pts',(26.7203516844276,-4.4065983348621,332.811412740351));
#66133=CARTESIAN_POINT('Ctrl Pts',(26.7125945746528,-4.46594864771926,332.935229735308));
#66134=CARTESIAN_POINT('Ctrl Pts',(26.7048374648781,-4.51998547835482,333.061208020967));
#66135=CARTESIAN_POINT('Ctrl Pts',(26.697076209952,-4.57405118454495,333.187253625395));
#66136=CARTESIAN_POINT('Ctrl Pts',(26.6893149550258,-4.62279761200044,333.315462456644));
#66137=CARTESIAN_POINT('Ctrl Pts',(26.6815537000996,-4.66607146383841,333.445342430999));
#66138=CARTESIAN_POINT('Ctrl Pts',(26.673780029695,-4.7094145397364,333.575430170984));
#66139=CARTESIAN_POINT('Ctrl Pts',(26.6660063592904,-4.74726743827675,333.707194020211));
#66140=CARTESIAN_POINT('Ctrl Pts',(26.6582326888857,-4.77952737723128,333.840128837846));
#66141=CARTESIAN_POINT('Ctrl Pts',(26.6508208847086,-4.81028560826618,333.966875507738));
#66142=CARTESIAN_POINT('Ctrl Pts',(26.6434090805315,-4.8359598094424,334.094686300082));
#66143=CARTESIAN_POINT('Ctrl Pts',(26.6359972763544,-4.85650484439102,334.223119211908));
#66144=CARTESIAN_POINT('Ctrl Pts',(26.6232769885537,-4.89176464769647,334.443538365258));
#66145=CARTESIAN_POINT('Ctrl Pts',(26.6105567007529,-4.91202471847816,334.666418079846));
#66146=CARTESIAN_POINT('Ctrl Pts',(26.5978364129523,-4.91702307292733,334.890149361402));
#66147=CARTESIAN_POINT('Ctrl Pts',(26.5958300674711,-4.91781145334917,334.925438047694));
#66148=CARTESIAN_POINT('Ctrl Pts',(26.5938237219899,-4.91822022182113,334.960747840938));
#66149=CARTESIAN_POINT('Ctrl Pts',(26.5918173765088,-4.91824843169319,334.996072322894));
#66150=CARTESIAN_POINT('',(24.8418173765385,-4.918249805682,334.998617462852));
#66151=CARTESIAN_POINT('Ctrl Pts',(26.59181737648,-4.9182484316936,334.996072323402));
#66152=CARTESIAN_POINT('Ctrl Pts',(26.5841678104404,-4.91835598707401,335.130753493758));
#66153=CARTESIAN_POINT('Ctrl Pts',(26.5765182444006,-4.91292722848413,335.265637886173));
#66154=CARTESIAN_POINT('Ctrl Pts',(26.5688686783609,-4.90193871815958,335.400224769234));
#66155=CARTESIAN_POINT('Ctrl Pts',(26.5612265307403,-4.89096086430546,335.534681132224));
#66156=CARTESIAN_POINT('Ctrl Pts',(26.5535843831196,-4.8744340150351,335.668840160233));
#66157=CARTESIAN_POINT('Ctrl Pts',(26.545942235499,-4.85238677358813,335.802200512345));
#66158=CARTESIAN_POINT('Ctrl Pts',(26.5381012774399,-4.82976597324687,335.939030233462));
#66159=CARTESIAN_POINT('Ctrl Pts',(26.5302603193808,-4.80133360103861,336.075018722663));
#66160=CARTESIAN_POINT('Ctrl Pts',(26.5224193613217,-4.76717746666161,336.209628895097));
#66161=CARTESIAN_POINT('Ctrl Pts',(26.5147854354675,-4.73392318888911,336.340684828293));
#66162=CARTESIAN_POINT('Ctrl Pts',(26.5071515096133,-4.69524372704886,336.470433902881));
#66163=CARTESIAN_POINT('Ctrl Pts',(26.4995175837591,-4.65127190295312,336.598390674178));
#66164=CARTESIAN_POINT('Ctrl Pts',(26.4918847006607,-4.6073060851869,336.726329967224));
#66165=CARTESIAN_POINT('Ctrl Pts',(26.4842518175623,-4.55804947356832,336.852477062175));
#66166=CARTESIAN_POINT('Ctrl Pts',(26.4766189344639,-4.50368444236786,336.976362695983));
#66167=CARTESIAN_POINT('Ctrl Pts',(26.4689853277714,-4.44931425738553,337.100260074097));
#66168=CARTESIAN_POINT('Ctrl Pts',(26.4613517210788,-4.38983485245253,337.221895195404));
#66169=CARTESIAN_POINT('Ctrl Pts',(26.4537181143863,-4.32547609201762,337.340820292095));
#66170=CARTESIAN_POINT('Ctrl Pts',(26.4457215416942,-4.25805717368356,337.465400090206));
#66171=CARTESIAN_POINT('Ctrl Pts',(26.4377249690021,-4.18528371274943,337.587005379117));
#66172=CARTESIAN_POINT('Ctrl Pts',(26.42972839631,-4.10747234174323,337.705153234905));
#66173=CARTESIAN_POINT('Ctrl Pts',(26.4220838676935,-4.03308656733136,337.818099705764));
#66174=CARTESIAN_POINT('Ctrl Pts',(26.4144393390768,-3.95409729883626,337.927886382928));
#66175=CARTESIAN_POINT('Ctrl Pts',(26.4067948104603,-3.87082327377047,338.034124296356));
#66176=CARTESIAN_POINT('Ctrl Pts',(26.3991452178191,-3.78749408484368,338.140432585792));
#66177=CARTESIAN_POINT('Ctrl Pts',(26.3914956251781,-3.69987475117922,338.243187127118));
#66178=CARTESIAN_POINT('Ctrl Pts',(26.3838460325369,-3.60832169700361,338.342034947967));
#66179=CARTESIAN_POINT('Ctrl Pts',(26.3761860433955,-3.51664421380359,338.4410171121));
#66180=CARTESIAN_POINT('Ctrl Pts',(26.3685260542541,-3.42102263016184,338.53608168211));
#66181=CARTESIAN_POINT('Ctrl Pts',(26.3608660651128,-3.32184738413784,338.626915082959));
#66182=CARTESIAN_POINT('Ctrl Pts',(26.3598304574353,-3.30843918677643,338.639195487742));
#66183=CARTESIAN_POINT('Ctrl Pts',(26.3587948497579,-3.29496607903849,338.651398618376));
#66184=CARTESIAN_POINT('Ctrl Pts',(26.3577592420804,-3.28142906622022,338.663523760789));
#66185=CARTESIAN_POINT('Ctrl Pts',(26.349984163302,-3.17979662047846,338.754556242985));
#66186=CARTESIAN_POINT('Ctrl Pts',(26.3422090845236,-3.0742126093444,338.841500181452));
#66187=CARTESIAN_POINT('Ctrl Pts',(26.3344340057451,-2.96503991377297,338.923993039269));
#66188=CARTESIAN_POINT('Ctrl Pts',(26.3266684946961,-2.85600156215402,339.006384384373));
#66189=CARTESIAN_POINT('Ctrl Pts',(26.3189029836472,-2.743383621755,339.084335313767));
#66190=CARTESIAN_POINT('Ctrl Pts',(26.3111374725982,-2.62758457925691,339.157521177499));
#66191=CARTESIAN_POINT('Ctrl Pts',(26.303379661076,-2.51190035184619,339.230634477234));
#66192=CARTESIAN_POINT('Ctrl Pts',(26.2956218495538,-2.39304162740545,339.298991906003));
#66193=CARTESIAN_POINT('Ctrl Pts',(26.2878640380316,-2.27143833809454,339.362310275386));
#66194=CARTESIAN_POINT('Ctrl Pts',(26.2801120645086,-2.14992655911526,339.425580995687));
#66195=CARTESIAN_POINT('Ctrl Pts',(26.2723600909856,-2.02567467158345,339.483820024704));
#66196=CARTESIAN_POINT('Ctrl Pts',(26.2646081174626,-1.89913953253943,339.536788742982));
#66197=CARTESIAN_POINT('Ctrl Pts',(26.256859426905,-1.77265798120192,339.589735028976));
#66198=CARTESIAN_POINT('Ctrl Pts',(26.2491107363474,-1.64389546137183,339.637415292864));
#66199=CARTESIAN_POINT('Ctrl Pts',(26.2413620457898,-1.51333105720149,339.67963803876));
#66200=CARTESIAN_POINT('Ctrl Pts',(26.233614967412,-1.38279381804611,339.721851999861));
#66201=CARTESIAN_POINT('Ctrl Pts',(26.2258678890341,-1.25045581192459,339.758610581329));
#66202=CARTESIAN_POINT('Ctrl Pts',(26.2181208106562,-1.11681324548536,339.789771522443));
#66203=CARTESIAN_POINT('Ctrl Pts',(26.2103736673504,-0.983169558992532,
339.820932724716));
#66204=CARTESIAN_POINT('Ctrl Pts',(26.2026265240447,-0.848221671037918,
339.846496104304));
#66205=CARTESIAN_POINT('Ctrl Pts',(26.1948793807389,-0.71247760711148,339.866370179288));
#66206=CARTESIAN_POINT('Ctrl Pts',(26.1871304957108,-0.576703025037542,
339.886248722387));
#66207=CARTESIAN_POINT('Ctrl Pts',(26.1793816106827,-0.440132297482836,
339.90043535905));
#66208=CARTESIAN_POINT('Ctrl Pts',(26.1716327256546,-0.303279828558278,
339.908890343865));
#66209=CARTESIAN_POINT('Ctrl Pts',(26.1638756158799,-0.16628210300944,339.917354302888));
#66210=CARTESIAN_POINT('Ctrl Pts',(26.1561185061052,-0.0290024294705457,
339.920074433289));
#66211=CARTESIAN_POINT('Ctrl Pts',(26.1483613963305,0.108042962821708,339.917063125554));
#66212=CARTESIAN_POINT('Ctrl Pts',(26.1406001414043,0.245161587789647,339.914050208672));
#66213=CARTESIAN_POINT('Ctrl Pts',(26.1328388864781,0.382045292173611,339.905299775877));
#66214=CARTESIAN_POINT('Ctrl Pts',(26.125077631552,0.518182699628412,339.890876174297));
#66215=CARTESIAN_POINT('Ctrl Pts',(26.1173039611473,0.65453788256825,339.876429499655));
#66216=CARTESIAN_POINT('Ctrl Pts',(26.1095302907427,0.790143996111655,339.856291578696));
#66217=CARTESIAN_POINT('Ctrl Pts',(26.1017566203381,0.92449870817882,339.830578143564));
#66218=CARTESIAN_POINT('Ctrl Pts',(26.0943448161609,1.0525991760772,339.806061675023));
#66219=CARTESIAN_POINT('Ctrl Pts',(26.0869330119837,1.17956184580616,339.776477156411));
#66220=CARTESIAN_POINT('Ctrl Pts',(26.0795212078065,1.30496573220709,339.741966627916));
#66221=CARTESIAN_POINT('Ctrl Pts',(26.0717461290281,1.43651603663802,339.705764635617));
#66222=CARTESIAN_POINT('Ctrl Pts',(26.0639710502496,1.56676661619699,339.664027142065));
#66223=CARTESIAN_POINT('Ctrl Pts',(26.0561959714712,1.69521623014514,339.616863112066));
#66224=CARTESIAN_POINT('Ctrl Pts',(26.0484304604222,1.82350777866566,339.569757120408));
#66225=CARTESIAN_POINT('Ctrl Pts',(26.0406649493732,1.9500024077694,339.517238012446));
#66226=CARTESIAN_POINT('Ctrl Pts',(26.0328994383241,2.07421146837759,339.459465197414));
#66227=CARTESIAN_POINT('Ctrl Pts',(26.0251416268019,2.19829737534065,339.401749664297));
#66228=CARTESIAN_POINT('Ctrl Pts',(26.0173838152797,2.32010187144078,339.33879095423));
#66229=CARTESIAN_POINT('Ctrl Pts',(26.0096260037575,2.43915415653436,339.270797356836));
#66230=CARTESIAN_POINT('Ctrl Pts',(26.0018740302345,2.55811685100805,339.202854926781));
#66231=CARTESIAN_POINT('Ctrl Pts',(25.9941220567115,2.67433111889856,339.129885344113));
#66232=CARTESIAN_POINT('Ctrl Pts',(25.9863700831884,2.78734906845822,339.052143658987));
#66233=CARTESIAN_POINT('Ctrl Pts',(25.9786213926308,2.90031915484929,338.97443489751));
#66234=CARTESIAN_POINT('Ctrl Pts',(25.9708727020732,3.01009529383858,338.891958274239));
#66235=CARTESIAN_POINT('Ctrl Pts',(25.9631240115155,3.11625719252611,338.805013031848));
#66236=CARTESIAN_POINT('Ctrl Pts',(25.9553769331377,3.22239700334379,338.71808587914));
#66237=CARTESIAN_POINT('Ctrl Pts',(25.9476298547598,3.32492376737622,338.626692204124));
#66238=CARTESIAN_POINT('Ctrl Pts',(25.939882776382,3.42344932865777,338.531172292117));
#66239=CARTESIAN_POINT('Ctrl Pts',(25.9321356330762,3.52197571567815,338.435651579561));
#66240=CARTESIAN_POINT('Ctrl Pts',(25.9243884897704,3.61650055242442,338.336004833114));
#66241=CARTESIAN_POINT('Ctrl Pts',(25.9166413464646,3.70667198805692,338.232609756134));
#66242=CARTESIAN_POINT('Ctrl Pts',(25.9088924614365,3.79686369614267,338.129191433746));
#66243=CARTESIAN_POINT('Ctrl Pts',(25.9011435764084,3.88269979867831,338.022023398464));
#66244=CARTESIAN_POINT('Ctrl Pts',(25.8933946913803,3.96386849931601,337.911516715156));
#66245=CARTESIAN_POINT('Ctrl Pts',(25.8856375816055,4.04512335325131,337.800892738912));
#66246=CARTESIAN_POINT('Ctrl Pts',(25.8778804718308,4.12170067739567,337.686923351341));
#66247=CARTESIAN_POINT('Ctrl Pts',(25.870123362056,4.19333152991012,337.570049365822));
#66248=CARTESIAN_POINT('Ctrl Pts',(25.8623621071299,4.2650006596618,337.453112926582));
#66249=CARTESIAN_POINT('Ctrl Pts',(25.8546008522037,4.33171786086935,337.333269137994));
#66250=CARTESIAN_POINT('Ctrl Pts',(25.8468395972775,4.39326050932327,337.21098284926));
#66251=CARTESIAN_POINT('Ctrl Pts',(25.8390659268729,4.45490160595802,337.088500942316));
#66252=CARTESIAN_POINT('Ctrl Pts',(25.8312922564681,4.51135144771493,336.963569083863));
#66253=CARTESIAN_POINT('Ctrl Pts',(25.8235185860635,4.56243551551167,336.836672324966));
#66254=CARTESIAN_POINT('Ctrl Pts',(25.8161067818864,4.61114160766195,336.715682640727));
#66255=CARTESIAN_POINT('Ctrl Pts',(25.8086949777095,4.65497014050902,336.592907142545));
#66256=CARTESIAN_POINT('Ctrl Pts',(25.8012831735325,4.69381273945129,336.468776711915));
#66257=CARTESIAN_POINT('Ctrl Pts',(25.793508094754,4.73455912987422,336.338562279114));
#66258=CARTESIAN_POINT('Ctrl Pts',(25.7857330159755,4.76994724349201,336.206445235331));
#66259=CARTESIAN_POINT('Ctrl Pts',(25.7779579371971,4.79979746100962,336.072906051705));
#66260=CARTESIAN_POINT('Ctrl Pts',(25.7701924261481,4.82961094593414,335.939531196547));
#66261=CARTESIAN_POINT('Ctrl Pts',(25.7624269150991,4.85390000967132,335.804738061425));
#66262=CARTESIAN_POINT('Ctrl Pts',(25.7546614040501,4.87253426679175,335.669023827259));
#66263=CARTESIAN_POINT('Ctrl Pts',(25.7469035925279,4.89115004799206,335.53344415415));
#66264=CARTESIAN_POINT('Ctrl Pts',(25.7391457810056,4.90412212751181,335.396945584207));
#66265=CARTESIAN_POINT('Ctrl Pts',(25.7313879694834,4.91137088356641,335.260036740781));
#66266=CARTESIAN_POINT('Ctrl Pts',(25.7236359959604,4.91861418470221,335.123230925601));
#66267=CARTESIAN_POINT('Ctrl Pts',(25.7158840224374,4.92014271462777,334.986015840234));
#66268=CARTESIAN_POINT('Ctrl Pts',(25.7081320489144,4.91592857053402,334.848906148678));
#66269=CARTESIAN_POINT('Ctrl Pts',(25.7003833583567,4.91171621113282,334.711854523158));
#66270=CARTESIAN_POINT('Ctrl Pts',(25.6926346677991,4.9017660268235,334.574908592552));
#66271=CARTESIAN_POINT('Ctrl Pts',(25.6848859772415,4.88610221254926,334.438583727506));
#66272=CARTESIAN_POINT('Ctrl Pts',(25.6771388988636,4.87044165726236,334.302287225986));
#66273=CARTESIAN_POINT('Ctrl Pts',(25.6693918204858,4.84906988114515,334.16661192108));
#66274=CARTESIAN_POINT('Ctrl Pts',(25.6616447421079,4.82206298391527,334.032068369329));
#66275=CARTESIAN_POINT('Ctrl Pts',(25.6538975988021,4.79505586034164,333.897523689973));
#66276=CARTESIAN_POINT('Ctrl Pts',(25.6461504554963,4.76241359838175,333.764111165923));
#66277=CARTESIAN_POINT('Ctrl Pts',(25.6384033121905,4.72426341016851,333.632331073014));
#66278=CARTESIAN_POINT('Ctrl Pts',(25.6306544271624,4.686104644983,333.500521353142));
#66279=CARTESIAN_POINT('Ctrl Pts',(25.6229055421343,4.64243559814119,333.370345170096));
#66280=CARTESIAN_POINT('Ctrl Pts',(25.6151566571062,4.59343321196466,333.242287170861));
#66281=CARTESIAN_POINT('Ctrl Pts',(25.6073995473314,4.54437881414915,333.114093249543));
#66282=CARTESIAN_POINT('Ctrl Pts',(25.5996424375567,4.48997990881064,332.988022368787));
#66283=CARTESIAN_POINT('Ctrl Pts',(25.591885327782,4.43046164546393,332.864539236939));
#66284=CARTESIAN_POINT('Ctrl Pts',(25.5841240728558,4.37091157746035,332.740990119653));
#66285=CARTESIAN_POINT('Ctrl Pts',(25.5763628179296,4.3062368846871,332.620031851169));
#66286=CARTESIAN_POINT('Ctrl Pts',(25.5686015630035,4.23670799402151,332.502103197509));
#66287=CARTESIAN_POINT('Ctrl Pts',(25.5608278925988,4.16706787979026,332.383985896437));
#66288=CARTESIAN_POINT('Ctrl Pts',(25.5530542221941,4.09255826317837,332.268908223001));
#66289=CARTESIAN_POINT('Ctrl Pts',(25.5452805517895,4.01349259168696,332.157279422987));
#66290=CARTESIAN_POINT('Ctrl Pts',(25.5378687476125,3.93810744622676,332.050846970471));
#66291=CARTESIAN_POINT('Ctrl Pts',(25.5304569434356,3.85858104450949,331.947549755237));
#66292=CARTESIAN_POINT('Ctrl Pts',(25.5230451392586,3.7752170762628,331.847712086501));
#66293=CARTESIAN_POINT('Ctrl Pts',(25.5152700604802,3.68776719160269,331.742981076217));
#66294=CARTESIAN_POINT('Ctrl Pts',(25.5074949817018,3.59581768974033,331.641726343238));
#66295=CARTESIAN_POINT('Ctrl Pts',(25.4997199029233,3.49967540680038,331.544358943765));
#66296=CARTESIAN_POINT('Ctrl Pts',(25.4919543918744,3.40365143306044,331.447111361076));
#66297=CARTESIAN_POINT('Ctrl Pts',(25.4841888808254,3.30344521614591,331.353741869352));
#66298=CARTESIAN_POINT('Ctrl Pts',(25.4764233697764,3.19940428706081,331.264629165607));
#66299=CARTESIAN_POINT('Ctrl Pts',(25.4686655582543,3.09546651486001,331.175604817367));
#66300=CARTESIAN_POINT('Ctrl Pts',(25.460907746732,2.98770189189243,331.090829110469));
#66301=CARTESIAN_POINT('Ctrl Pts',(25.4531499352099,2.876495042469,331.010644245852));
#66302=CARTESIAN_POINT('Ctrl Pts',(25.4453979616869,2.76537187972604,330.930519722889));
#66303=CARTESIAN_POINT('Ctrl Pts',(25.4376459881639,2.65081196233557,330.854979393372));
#66304=CARTESIAN_POINT('Ctrl Pts',(25.429894014641,2.53323298242315,330.784325235592));
#66305=CARTESIAN_POINT('Ctrl Pts',(25.4221453240834,2.41570379727869,330.71370099989));
#66306=CARTESIAN_POINT('Ctrl Pts',(25.4143966335258,2.29515842694781,330.647959021147));
#66307=CARTESIAN_POINT('Ctrl Pts',(25.4066479429682,2.1720433508746,330.587357849947));
#66308=CARTESIAN_POINT('Ctrl Pts',(25.3989008645903,2.04895388992109,330.526769287328));
#66309=CARTESIAN_POINT('Ctrl Pts',(25.3911537862125,1.9232961371507,330.471319577279));
#66310=CARTESIAN_POINT('Ctrl Pts',(25.3834067078347,1.79554061237672,330.421221017367));
#66311=CARTESIAN_POINT('Ctrl Pts',(25.3756595645289,1.6677840168884,330.37112203758));
#66312=CARTESIAN_POINT('Ctrl Pts',(25.3679124212231,1.53792997822426,330.326374440081));
#66313=CARTESIAN_POINT('Ctrl Pts',(25.3601652779173,1.40646803079301,330.287141977435));
#66314=CARTESIAN_POINT('Ctrl Pts',(25.3524163928893,1.27497652792514,330.247900694498));
#66315=CARTESIAN_POINT('Ctrl Pts',(25.3446675078612,1.14187677143915,330.214177125471));
#66316=CARTESIAN_POINT('Ctrl Pts',(25.3369186228331,1.00767206496916,330.186084746074));
#66317=CARTESIAN_POINT('Ctrl Pts',(25.3291615130584,0.873324912236947,330.157962549136));
#66318=CARTESIAN_POINT('Ctrl Pts',(25.3214044032837,0.737870849918725,330.135483561662));
#66319=CARTESIAN_POINT('Ctrl Pts',(25.313647293509,0.601822502496497,330.118709930972));
#66320=CARTESIAN_POINT('Ctrl Pts',(25.3058860385829,0.465701455187667,330.101927336991));
#66321=CARTESIAN_POINT('Ctrl Pts',(25.2981247836567,0.328985879395393,330.090856206257));
#66322=CARTESIAN_POINT('Ctrl Pts',(25.2903635287306,0.192191086329997,330.085506572511));
#66323=CARTESIAN_POINT('Ctrl Pts',(25.2825898583259,0.0551774661768272,
330.080148381094));
#66324=CARTESIAN_POINT('Ctrl Pts',(25.2748161879213,-0.0819152333988373,
330.080529975044));
#66325=CARTESIAN_POINT('Ctrl Pts',(25.2670425175166,-0.218573244457722,
330.086609236046));
#66326=CARTESIAN_POINT('Ctrl Pts',(25.2596307133393,-0.348869792228236,
330.092405505986));
#66327=CARTESIAN_POINT('Ctrl Pts',(25.252218909162,-0.478770923467465,330.103380903456));
#66328=CARTESIAN_POINT('Ctrl Pts',(25.2448071049847,-0.607839575699074,
330.11945555161));
#66329=CARTESIAN_POINT('Ctrl Pts',(25.2370320262062,-0.743234267048079,
330.136318066153));
#66330=CARTESIAN_POINT('Ctrl Pts',(25.2292569474278,-0.878140683704208,
330.158845617916));
#66331=CARTESIAN_POINT('Ctrl Pts',(25.2214818686493,-1.01204711310582,330.187002627951));
#66332=CARTESIAN_POINT('Ctrl Pts',(25.2137163576003,-1.14578876212116,330.215124988992));
#66333=CARTESIAN_POINT('Ctrl Pts',(25.2059508465513,-1.27853249346685,330.24886294509));
#66334=CARTESIAN_POINT('Ctrl Pts',(25.1981853355023,-1.40977178377825,330.288129184691));
#66335=CARTESIAN_POINT('Ctrl Pts',(25.1904275239801,-1.54088094995148,330.327356491701));
#66336=CARTESIAN_POINT('Ctrl Pts',(25.1826697124578,-1.67048827151333,330.372101062781));
#66337=CARTESIAN_POINT('Ctrl Pts',(25.1749119009356,-1.79809784211041,330.422224643705));
#66338=CARTESIAN_POINT('Ctrl Pts',(25.1671599274126,-1.92561138245871,330.472310505045));
#66339=CARTESIAN_POINT('Ctrl Pts',(25.1594079538895,-2.05112980187823,330.527767176804));
#66340=CARTESIAN_POINT('Ctrl Pts',(25.1516559803665,-2.17417312320725,330.58840683054));
#66341=CARTESIAN_POINT('Ctrl Pts',(25.1439072898089,-2.29716433561631,330.649020803348));
#66342=CARTESIAN_POINT('Ctrl Pts',(25.1361585992513,-2.41768218486336,330.71481322001));
#66343=CARTESIAN_POINT('Ctrl Pts',(25.1284099086937,-2.53526763459921,330.785548542995));
#66344=CARTESIAN_POINT('Ctrl Pts',(25.1206628303159,-2.65282861970047,330.856269148905));
#66345=CARTESIAN_POINT('Ctrl Pts',(25.112915751938,-2.76745808411275,330.93193041419));
#66346=CARTESIAN_POINT('Ctrl Pts',(25.1051686735602,-2.87872287701492,331.012251555094));
#66347=CARTESIAN_POINT('Ctrl Pts',(25.0974215302544,-2.98998860242262,331.092573369166));
#66348=CARTESIAN_POINT('Ctrl Pts',(25.0896743869486,-3.09788928315148,331.17755490797));
#66349=CARTESIAN_POINT('Ctrl Pts',(25.0819272436428,-3.20202230101834,331.266873127487));
#66350=CARTESIAN_POINT('Ctrl Pts',(25.0741783586147,-3.30617873019913,331.356211427636));
#66351=CARTESIAN_POINT('Ctrl Pts',(25.0664294735865,-3.40656551435227,331.449888094166));
#66352=CARTESIAN_POINT('Ctrl Pts',(25.0586805885584,-3.50281486284738,331.547541296537));
#66353=CARTESIAN_POINT('Ctrl Pts',(25.0509234787837,-3.59916637139516,331.645298149026));
#66354=CARTESIAN_POINT('Ctrl Pts',(25.0431663690089,-3.69137139700285,331.74703968985));
#66355=CARTESIAN_POINT('Ctrl Pts',(25.0354092592342,-3.77910026814199,331.852368473625));
#66356=CARTESIAN_POINT('Ctrl Pts',(25.027648004308,-3.8668760187849,331.957753541735));
#66357=CARTESIAN_POINT('Ctrl Pts',(25.0198867493818,-3.95017061161098,332.066729362017));
#66358=CARTESIAN_POINT('Ctrl Pts',(25.0121254944557,-4.02869674456863,332.178868028113));
#66359=CARTESIAN_POINT('Ctrl Pts',(25.004351824051,-4.10734849374729,332.29118607953));
#66360=CARTESIAN_POINT('Ctrl Pts',(24.9965781536464,-4.18121632937148,332.40667675773));
#66361=CARTESIAN_POINT('Ctrl Pts',(24.9888044832417,-4.25005764031842,332.524885231657));
#66362=CARTESIAN_POINT('Ctrl Pts',(24.9813926790647,-4.31569437167778,332.637591072682));
#66363=CARTESIAN_POINT('Ctrl Pts',(24.9739808748877,-4.3767618816319,332.752767122594));
#66364=CARTESIAN_POINT('Ctrl Pts',(24.9665690707106,-4.43309082073933,332.870002620289));
#66365=CARTESIAN_POINT('Ctrl Pts',(24.9581780317219,-4.49686184233671,333.002727070171));
#66366=CARTESIAN_POINT('Ctrl Pts',(24.9497869927331,-4.55473719931768,333.138460421256));
#66367=CARTESIAN_POINT('Ctrl Pts',(24.9413959537443,-4.60644548241803,333.276676733747));
#66368=CARTESIAN_POINT('Ctrl Pts',(24.9330321278271,-4.65798606981271,333.414444795383));
#66369=CARTESIAN_POINT('Ctrl Pts',(24.9246683019098,-4.70339937041807,333.554679484578));
#66370=CARTESIAN_POINT('Ctrl Pts',(24.9163044759925,-4.74246172510439,333.696834681086));
#66371=CARTESIAN_POINT('Ctrl Pts',(24.9079570496449,-4.78144748735369,333.838711143426));
#66372=CARTESIAN_POINT('Ctrl Pts',(24.8996096232974,-4.81410704695216,333.982500326997));
#66373=CARTESIAN_POINT('Ctrl Pts',(24.8912621969498,-4.84026523280527,334.127637954404));
#66374=CARTESIAN_POINT('Ctrl Pts',(24.8829409241885,-4.86634146161674,334.272320846508));
#66375=CARTESIAN_POINT('Ctrl Pts',(24.8746196514271,-4.88595688602604,334.418343470128));
#66376=CARTESIAN_POINT('Ctrl Pts',(24.8662983786658,-4.89898671254474,334.565129613781));
#66377=CARTESIAN_POINT('Ctrl Pts',(24.8581380446233,-4.91176453391375,334.709076819859));
#66378=CARTESIAN_POINT('Ctrl Pts',(24.8499777105809,-4.91820908518151,334.853757996438));
#66379=CARTESIAN_POINT('Ctrl Pts',(24.8418173765385,-4.918249805682,334.998617462852));
#66380=CARTESIAN_POINT('',(23.0918173764689,-4.91824794611119,335.004494782867));
#66381=CARTESIAN_POINT('Ctrl Pts',(24.8418173765088,-4.91824980568215,334.998617463379));
#66382=CARTESIAN_POINT('Ctrl Pts',(24.8338553286311,-4.91828953670899,335.139957021433));
#66383=CARTESIAN_POINT('Ctrl Pts',(24.8258932807534,-4.91223224148295,335.281236635687));
#66384=CARTESIAN_POINT('Ctrl Pts',(24.8179312328757,-4.90011963284472,335.421913079093));
#66385=CARTESIAN_POINT('Ctrl Pts',(24.8099637414546,-4.88799874298139,335.562685701062));
#66386=CARTESIAN_POINT('Ctrl Pts',(24.8019962500334,-4.86981431778907,335.702853972241));
#66387=CARTESIAN_POINT('Ctrl Pts',(24.7940287586123,-4.8456597466068,335.841881632187));
#66388=CARTESIAN_POINT('Ctrl Pts',(24.7860545473129,-4.8214848031681,335.981026549737));
#66389=CARTESIAN_POINT('Ctrl Pts',(24.7780803360135,-4.79132973732307,336.11902858484));
#66390=CARTESIAN_POINT('Ctrl Pts',(24.7701061247141,-4.75533864122688,336.25536348113));
#66391=CARTESIAN_POINT('Ctrl Pts',(24.7621181777571,-4.71928555011239,336.391933215625));
#66392=CARTESIAN_POINT('Ctrl Pts',(24.7541302308,-4.67737643562674,336.526829726102));
#66393=CARTESIAN_POINT('Ctrl Pts',(24.7461422838429,-4.6298050529789,336.659544586298));
#66394=CARTESIAN_POINT('Ctrl Pts',(24.7381465940739,-4.58218755882447,336.792388088586));
#66395=CARTESIAN_POINT('Ctrl Pts',(24.7301509043049,-4.52889698612354,336.923045391491));
#66396=CARTESIAN_POINT('Ctrl Pts',(24.7221552145359,-4.47017434920947,337.051030070518));
#66397=CARTESIAN_POINT('Ctrl Pts',(24.7141449758748,-4.41134486106237,337.179247629428));
#66398=CARTESIAN_POINT('Ctrl Pts',(24.7061347372136,-4.34706372268284,337.304782528415));
#66399=CARTESIAN_POINT('Ctrl Pts',(24.6981244985525,-4.27761732016084,337.427173896687));
#66400=CARTESIAN_POINT('Ctrl Pts',(24.6948600111806,-4.24931517915742,337.477053194054));
#66401=CARTESIAN_POINT('Ctrl Pts',(24.6915955238087,-4.22015563878822,337.526410738232));
#66402=CARTESIAN_POINT('Ctrl Pts',(24.6883310364368,-4.1901600519002,337.575216845619));
#66403=CARTESIAN_POINT('Ctrl Pts',(24.6805559576583,-4.11871911049332,337.691459087224));
#66404=CARTESIAN_POINT('Ctrl Pts',(24.6727808788798,-4.04232447413337,337.804909919654));
#66405=CARTESIAN_POINT('Ctrl Pts',(24.6650058001013,-3.96122052587272,337.915118352298));
#66406=CARTESIAN_POINT('Ctrl Pts',(24.6572402890523,-3.88021638118385,338.02519116645));
#66407=CARTESIAN_POINT('Ctrl Pts',(24.6494747780032,-3.79451468465992,338.132029207925));
#66408=CARTESIAN_POINT('Ctrl Pts',(24.6417092669542,-3.70440475347745,338.2352076417));
#66409=CARTESIAN_POINT('Ctrl Pts',(24.6339514554319,-3.61438416655415,338.338283773757));
#66410=CARTESIAN_POINT('Ctrl Pts',(24.6261936439097,-3.51996429852614,338.43770722655));
#66411=CARTESIAN_POINT('Ctrl Pts',(24.6184358323875,-3.42147643301484,338.533083933453));
#66412=CARTESIAN_POINT('Ctrl Pts',(24.6106838588645,-3.32306268274556,338.62838886636));
#66413=CARTESIAN_POINT('Ctrl Pts',(24.6029318853415,-3.22058730801388,338.719652844082));
#66414=CARTESIAN_POINT('Ctrl Pts',(24.5951799118184,-3.11442011257202,338.806516836283));
#66415=CARTESIAN_POINT('Ctrl Pts',(24.5874312212608,-3.00829787900045,338.893344041532));
#66416=CARTESIAN_POINT('Ctrl Pts',(24.5796825307031,-2.89848723627722,338.975774720422));
#66417=CARTESIAN_POINT('Ctrl Pts',(24.5719338401454,-2.78539273445925,339.053488667472));
#66418=CARTESIAN_POINT('Ctrl Pts',(24.5641867617676,-2.67232176289697,339.131186445486));
#66419=CARTESIAN_POINT('Ctrl Pts',(24.5564396833898,-2.55596861318709,339.204169222417));
#66420=CARTESIAN_POINT('Ctrl Pts',(24.5486926050119,-2.43676829154808,339.27215909767));
#66421=CARTESIAN_POINT('Ctrl Pts',(24.5409454617061,-2.31756697089557,339.340149542744));
#66422=CARTESIAN_POINT('Ctrl Pts',(24.5331983184002,-2.19551877024599,339.403146809016));
#66423=CARTESIAN_POINT('Ctrl Pts',(24.5254511750944,-2.07108450904925,339.46091829323));
#66424=CARTESIAN_POINT('Ctrl Pts',(24.5177022900663,-1.94662227238861,339.518702765701));
#66425=CARTESIAN_POINT('Ctrl Pts',(24.5099534050381,-1.81977326218987,339.571258953695));
#66426=CARTESIAN_POINT('Ctrl Pts',(24.50220452001,-1.69101917016387,339.618402021115));
#66427=CARTESIAN_POINT('Ctrl Pts',(24.4944474102352,-1.56212841721432,339.665595126674));
#66428=CARTESIAN_POINT('Ctrl Pts',(24.4866903004605,-1.43132891077975,339.707363499794));
#66429=CARTESIAN_POINT('Ctrl Pts',(24.4789331906857,-1.29911896447607,339.743571753293));
#66430=CARTESIAN_POINT('Ctrl Pts',(24.4711719357595,-1.16683836940443,339.779799355325));
#66431=CARTESIAN_POINT('Ctrl Pts',(24.4634106808333,-1.03314621345038,339.810460830121));
#66432=CARTESIAN_POINT('Ctrl Pts',(24.4556494259071,-0.89855098046584,339.835471972621));
#66433=CARTESIAN_POINT('Ctrl Pts',(24.4478757555024,-0.76374043897319,339.860523124798));
#66434=CARTESIAN_POINT('Ctrl Pts',(24.4401020850977,-0.62802432080506,339.879905827409));
#66435=CARTESIAN_POINT('Ctrl Pts',(24.432328414693,-0.491917099767684,339.893587705299));
#66436=CARTESIAN_POINT('Ctrl Pts',(24.4249166105163,-0.362145702621913,
339.906632688482));
#66437=CARTESIAN_POINT('Ctrl Pts',(24.4175048063396,-0.232019082134269,
339.914495632242));
#66438=CARTESIAN_POINT('Ctrl Pts',(24.4100930021629,-0.101981250092211,
339.917192581863));
#66439=CARTESIAN_POINT('Ctrl Pts',(24.4023179233844,0.034430123467639,339.920021717019));
#66440=CARTESIAN_POINT('Ctrl Pts',(24.394542844606,0.171174870082267,339.917174592731));
#66441=CARTESIAN_POINT('Ctrl Pts',(24.3867677658275,0.307741492433349,339.908612659024));
#66442=CARTESIAN_POINT('Ctrl Pts',(24.3790022547785,0.444140060861186,339.900061261322));
#66443=CARTESIAN_POINT('Ctrl Pts',(24.3712367437296,0.580360554778097,339.885809070958));
#66444=CARTESIAN_POINT('Ctrl Pts',(24.3634712326806,0.71588915522387,339.865869478308));
#66445=CARTESIAN_POINT('Ctrl Pts',(24.3557134211583,0.851283378667813,339.845949655823));
#66446=CARTESIAN_POINT('Ctrl Pts',(24.3479556096361,0.98598668962775,339.820353709662));
#66447=CARTESIAN_POINT('Ctrl Pts',(24.3401977981139,1.1194884324956,339.789146971227));
#66448=CARTESIAN_POINT('Ctrl Pts',(24.3324458245909,1.25288971106872,339.757963716852));
#66449=CARTESIAN_POINT('Ctrl Pts',(24.3246938510679,1.38509084227026,339.721178163095));
#66450=CARTESIAN_POINT('Ctrl Pts',(24.3169418775448,1.51558978779994,339.678906993905));
#66451=CARTESIAN_POINT('Ctrl Pts',(24.3091931869872,1.64603346694818,339.636653726581));
#66452=CARTESIAN_POINT('Ctrl Pts',(24.3014444964296,1.77477602311863,339.588919584627));
#66453=CARTESIAN_POINT('Ctrl Pts',(24.293695805872,1.90132926344153,339.535871481257));
#66454=CARTESIAN_POINT('Ctrl Pts',(24.2859487274942,2.02785617330561,339.482834414988));
#66455=CARTESIAN_POINT('Ctrl Pts',(24.2782016491163,2.152194313096,339.424485737461));
#66456=CARTESIAN_POINT('Ctrl Pts',(24.2704545707385,2.27387458344803,339.361040866725));
#66457=CARTESIAN_POINT('Ctrl Pts',(24.2627074274327,2.39555587359792,339.297595464261));
#66458=CARTESIAN_POINT('Ctrl Pts',(24.2549602841269,2.51457890328879,339.229053964113));
#66459=CARTESIAN_POINT('Ctrl Pts',(24.2472131408211,2.63049869563477,339.155678004221));
#66460=CARTESIAN_POINT('Ctrl Pts',(24.239464255793,2.7464445492108,339.082285547855));
#66461=CARTESIAN_POINT('Ctrl Pts',(24.231715370765,2.85928544694446,339.004056677972));
#66462=CARTESIAN_POINT('Ctrl Pts',(24.2239664857369,2.96860528519365,338.92129643399));
#66463=CARTESIAN_POINT('Ctrl Pts',(24.2162093759622,3.07804115664909,338.838448347429));
#66464=CARTESIAN_POINT('Ctrl Pts',(24.2084522661874,3.18394819090044,338.751059515348));
#66465=CARTESIAN_POINT('Ctrl Pts',(24.2006951564127,3.28594287188699,338.659475714525));
#66466=CARTESIAN_POINT('Ctrl Pts',(24.1929339014865,3.38799205556984,338.567842974246));
#66467=CARTESIAN_POINT('Ctrl Pts',(24.1851726465604,3.48612444069997,338.472011071475));
#66468=CARTESIAN_POINT('Ctrl Pts',(24.1774113916343,3.57999404765856,338.372362032942));
#66469=CARTESIAN_POINT('Ctrl Pts',(24.1696377212296,3.67401381539625,338.272553588423));
#66470=CARTESIAN_POINT('Ctrl Pts',(24.1618640508249,3.76375692246318,338.168916101842));
#66471=CARTESIAN_POINT('Ctrl Pts',(24.1540903804203,3.84891773260542,338.061864685145));
#66472=CARTESIAN_POINT('Ctrl Pts',(24.1466785762431,3.93011428654773,337.959796537649));
#66473=CARTESIAN_POINT('Ctrl Pts',(24.139266772066,4.0071453847187,337.85462537639));
#66474=CARTESIAN_POINT('Ctrl Pts',(24.1318549678888,4.07978423968329,337.746733263375));
#66475=CARTESIAN_POINT('Ctrl Pts',(24.1240798891104,4.15598334130899,337.633553036509));
#66476=CARTESIAN_POINT('Ctrl Pts',(24.116304810332,4.22758956255946,337.517020719439));
#66477=CARTESIAN_POINT('Ctrl Pts',(24.1085297315536,4.29429368538976,337.397545579571));
#66478=CARTESIAN_POINT('Ctrl Pts',(24.1007642205046,4.36091572455051,337.278217461469));
#66479=CARTESIAN_POINT('Ctrl Pts',(24.0929987094556,4.42264747920467,337.155954064));
#66480=CARTESIAN_POINT('Ctrl Pts',(24.0852331984065,4.47922215268417,337.031194714793));
#66481=CARTESIAN_POINT('Ctrl Pts',(24.0774753868844,4.53574073221009,336.906559064844));
#66482=CARTESIAN_POINT('Ctrl Pts',(24.0697175753621,4.58711224585203,336.779432741726));
#66483=CARTESIAN_POINT('Ctrl Pts',(24.06195976384,4.63311528712954,336.650280521204));
#66484=CARTESIAN_POINT('Ctrl Pts',(24.0542077903169,4.6790837096597,336.521225491824));
#66485=CARTESIAN_POINT('Ctrl Pts',(24.046455816794,4.7196915705131,336.390147966317));
#66486=CARTESIAN_POINT('Ctrl Pts',(24.038703843271,4.75476530997945,336.257533263781));
#66487=CARTESIAN_POINT('Ctrl Pts',(24.0309551527133,4.78982419569626,336.12497472365));
#66488=CARTESIAN_POINT('Ctrl Pts',(24.0232064621557,4.81935352175403,335.990880678369));
#66489=CARTESIAN_POINT('Ctrl Pts',(24.0154577715981,4.84322945986104,335.855751986053));
#66490=CARTESIAN_POINT('Ctrl Pts',(24.0077106932203,4.8671004303797,335.720651408391));
#66491=CARTESIAN_POINT('Ctrl Pts',(23.9999636148425,4.88532028459383,335.584516996546));
#66492=CARTESIAN_POINT('Ctrl Pts',(23.9922165364647,4.89781631555561,335.447859801252));
#66493=CARTESIAN_POINT('Ctrl Pts',(23.9844693931589,4.91031245124615,335.311201460638));
#66494=CARTESIAN_POINT('Ctrl Pts',(23.976722249853,4.91708463240899,335.174020717086));
#66495=CARTESIAN_POINT('Ctrl Pts',(23.9689751065472,4.91811207344259,335.036833348452));
#66496=CARTESIAN_POINT('Ctrl Pts',(23.9612262215191,4.91913974546676,334.899615137185));
#66497=CARTESIAN_POINT('Ctrl Pts',(23.9534773364911,4.91442010441552,334.76239068866));
#66498=CARTESIAN_POINT('Ctrl Pts',(23.945728451463,4.90398448688619,334.625674987638));
#66499=CARTESIAN_POINT('Ctrl Pts',(23.9379713416883,4.89353779288461,334.488814175159));
#66500=CARTESIAN_POINT('Ctrl Pts',(23.9302142319135,4.87736303280648,334.352463579221));
#66501=CARTESIAN_POINT('Ctrl Pts',(23.9224571221388,4.85554343517451,334.217132826315));
#66502=CARTESIAN_POINT('Ctrl Pts',(23.9146958672126,4.8337121778472,334.081729756982));
#66503=CARTESIAN_POINT('Ctrl Pts',(23.9069346122864,4.80623015075202,333.94734799934));
#66504=CARTESIAN_POINT('Ctrl Pts',(23.8991733573603,4.77323137889276,333.814485231617));
#66505=CARTESIAN_POINT('Ctrl Pts',(23.8913996869556,4.74017981975284,333.681409926766));
#66506=CARTESIAN_POINT('Ctrl Pts',(23.883626016551,4.70159399097006,333.549858842741));
#66507=CARTESIAN_POINT('Ctrl Pts',(23.8758523461463,4.65765757172184,333.420313636483));
#66508=CARTESIAN_POINT('Ctrl Pts',(23.8684405419692,4.61576640335982,333.296798790741));
#66509=CARTESIAN_POINT('Ctrl Pts',(23.8610287377921,4.56901167739254,333.175107546826));
#66510=CARTESIAN_POINT('Ctrl Pts',(23.8536169336149,4.51759195021922,333.055637370804));
#66511=CARTESIAN_POINT('Ctrl Pts',(23.8458418548365,4.46365198904594,332.930311605572));
#66512=CARTESIAN_POINT('Ctrl Pts',(23.8380667760581,4.40440771259694,332.807034083082));
#66513=CARTESIAN_POINT('Ctrl Pts',(23.8302916972796,4.34003594693644,332.686286309458));
#66514=CARTESIAN_POINT('Ctrl Pts',(23.8225261862306,4.2757433948317,332.565687123658));
#66515=CARTESIAN_POINT('Ctrl Pts',(23.8147606751816,4.20633609013593,332.447611834338));
#66516=CARTESIAN_POINT('Ctrl Pts',(23.8069951641326,4.13203909383756,332.332522541895));
#66517=CARTESIAN_POINT('Ctrl Pts',(23.7992373526104,4.05781576322758,332.217547360821));
#66518=CARTESIAN_POINT('Ctrl Pts',(23.7914795410882,3.97871259972482,332.105552611091));
#66519=CARTESIAN_POINT('Ctrl Pts',(23.7837217295661,3.8950006274356,331.996975994972));
#66520=CARTESIAN_POINT('Ctrl Pts',(23.775969756043,3.81135165105997,331.888481086199));
#66521=CARTESIAN_POINT('Ctrl Pts',(23.76821778252,3.72310100703136,331.783399499398));
#66522=CARTESIAN_POINT('Ctrl Pts',(23.760465808997,3.63056288741391,331.682139818643));
#66523=CARTESIAN_POINT('Ctrl Pts',(23.7527171184394,3.53806395774507,331.580923021423));
#66524=CARTESIAN_POINT('Ctrl Pts',(23.7449684278818,3.44128142701886,331.483525198944));
#66525=CARTESIAN_POINT('Ctrl Pts',(23.7372197373241,3.3405694669172,331.390321524124));
#66526=CARTESIAN_POINT('Ctrl Pts',(23.7294726589463,3.23987846078013,331.297137241108));
#66527=CARTESIAN_POINT('Ctrl Pts',(23.7217255805685,3.13525993813002,331.208145635356));
#66528=CARTESIAN_POINT('Ctrl Pts',(23.7139785021906,3.02710430652878,331.123684406567));
#66529=CARTESIAN_POINT('Ctrl Pts',(23.7062313588848,2.91894776847888,331.039222469911));
#66530=CARTESIAN_POINT('Ctrl Pts',(23.698484215579,2.80725437041722,330.959291226527));
#66531=CARTESIAN_POINT('Ctrl Pts',(23.6907370722732,2.69244659266633,330.884187272465));
#66532=CARTESIAN_POINT('Ctrl Pts',(23.6829881872451,2.57761300369018,330.80906643344));
#66533=CARTESIAN_POINT('Ctrl Pts',(23.675239302217,2.45966396878477,330.738775257255));
#66534=CARTESIAN_POINT('Ctrl Pts',(23.667490417189,2.33904950765398,330.673566080102));
#66535=CARTESIAN_POINT('Ctrl Pts',(23.6597333074142,2.21830702508764,330.608287689254));
#66536=CARTESIAN_POINT('Ctrl Pts',(23.6519761976395,2.09489380926462,330.54810225882));
#66537=CARTESIAN_POINT('Ctrl Pts',(23.6442190878648,1.96928345570421,330.493215588295));
#66538=CARTESIAN_POINT('Ctrl Pts',(23.6364578329386,1.84360597998719,330.438299588088));
#66539=CARTESIAN_POINT('Ctrl Pts',(23.6286965780125,1.71572939129793,330.388688131092));
#66540=CARTESIAN_POINT('Ctrl Pts',(23.6209353230863,1.58614472649503,330.344537835068));
#66541=CARTESIAN_POINT('Ctrl Pts',(23.6131616526817,1.45635276845982,330.300316912959));
#66542=CARTESIAN_POINT('Ctrl Pts',(23.605387982277,1.32484764937521,330.261574719609));
#66543=CARTESIAN_POINT('Ctrl Pts',(23.5976143118723,1.19213380417996,330.228417447489));
#66544=CARTESIAN_POINT('Ctrl Pts',(23.5902025076952,1.06559782040747,330.196803654362));
#66545=CARTESIAN_POINT('Ctrl Pts',(23.5827907035181,0.937963392224171,330.170266586172));
#66546=CARTESIAN_POINT('Ctrl Pts',(23.575378899341,0.809672207586631,330.148854364301));
#66547=CARTESIAN_POINT('Ctrl Pts',(23.5676038205626,0.675093089830752,330.126392665653));
#66548=CARTESIAN_POINT('Ctrl Pts',(23.5598287417841,0.539365913735656,330.109499900557));
#66549=CARTESIAN_POINT('Ctrl Pts',(23.5520536630057,0.402991278805547,330.098287942799));
#66550=CARTESIAN_POINT('Ctrl Pts',(23.5442881519567,0.266784461545384,330.087089782069));
#66551=CARTESIAN_POINT('Ctrl Pts',(23.5365226409077,0.129932156568909,330.081558551118));
#66552=CARTESIAN_POINT('Ctrl Pts',(23.5287571298587,-0.00705525262612259,
330.081755060399));
#66553=CARTESIAN_POINT('Ctrl Pts',(23.5209993183366,-0.143906838405085,
330.081951374841));
#66554=CARTESIAN_POINT('Ctrl Pts',(23.5132415068143,-0.280892873466163,
330.087864127286));
#66555=CARTESIAN_POINT('Ctrl Pts',(23.5054836952922,-0.417498617938304,
330.099502273593));
#66556=CARTESIAN_POINT('Ctrl Pts',(23.4977317217692,-0.554001562256641,
330.111131661826));
#66557=CARTESIAN_POINT('Ctrl Pts',(23.4899797482462,-0.690124397719518,
330.128477834937));
#66558=CARTESIAN_POINT('Ctrl Pts',(23.4822277747232,-0.825353509908196,
330.151497690401));
#66559=CARTESIAN_POINT('Ctrl Pts',(23.4744790841656,-0.960525352487391,
330.174507796944));
#66560=CARTESIAN_POINT('Ctrl Pts',(23.4667303936079,-1.09480384005777,330.203186741366));
#66561=CARTESIAN_POINT('Ctrl Pts',(23.4589817030503,-1.22768181908871,330.237439720741));
#66562=CARTESIAN_POINT('Ctrl Pts',(23.4512346246725,-1.36053215174629,330.271685573496));
#66563=CARTESIAN_POINT('Ctrl Pts',(23.4434875462947,-1.49198217719144,330.311503056921));
#66564=CARTESIAN_POINT('Ctrl Pts',(23.4357404679169,-1.62153664460972,330.356746617652));
#66565=CARTESIAN_POINT('Ctrl Pts',(23.4279933246111,-1.75109219781887,330.401990557567));
#66566=CARTESIAN_POINT('Ctrl Pts',(23.4202461813053,-1.87875179229501,330.452660536622));
#66567=CARTESIAN_POINT('Ctrl Pts',(23.4124990379995,-2.00403738574771,330.508561787242));
#66568=CARTESIAN_POINT('Ctrl Pts',(23.4047501529715,-2.12935114606187,330.56447560565));
#66569=CARTESIAN_POINT('Ctrl Pts',(23.3970012679434,-2.25228948641384,330.625622876693));
#66570=CARTESIAN_POINT('Ctrl Pts',(23.3892523829153,-2.37239668043311,330.691761722795));
#66571=CARTESIAN_POINT('Ctrl Pts',(23.3814952731406,-2.49263135746923,330.757970769352));
#66572=CARTESIAN_POINT('Ctrl Pts',(23.3737381633659,-2.61002854245246,330.829181785596));
#66573=CARTESIAN_POINT('Ctrl Pts',(23.3659810535912,-2.72415888448473,330.905107884866));
#66574=CARTESIAN_POINT('Ctrl Pts',(23.358219798665,-2.83835021412237,330.981074556617));
#66575=CARTESIAN_POINT('Ctrl Pts',(23.3504585437389,-2.94927090642088,331.061761102088));
#66576=CARTESIAN_POINT('Ctrl Pts',(23.3426972888127,-3.05652352994429,331.146839352765));
#66577=CARTESIAN_POINT('Ctrl Pts',(23.3349236184081,-3.16394772271194,331.232053700918));
#66578=CARTESIAN_POINT('Ctrl Pts',(23.3271499480034,-3.2676918253267,331.321673537246));
#66579=CARTESIAN_POINT('Ctrl Pts',(23.3193762775988,-3.36739355958634,331.415332138488));
#66580=CARTESIAN_POINT('Ctrl Pts',(23.3119644734215,-3.46245415413123,331.504630909311));
#66581=CARTESIAN_POINT('Ctrl Pts',(23.3045526692443,-3.55384005366963,331.597600692638));
#66582=CARTESIAN_POINT('Ctrl Pts',(23.2971408650671,-3.64127176920603,331.693896104887));
#66583=CARTESIAN_POINT('Ctrl Pts',(23.2894457560932,-3.73204542737938,331.793872260924));
#66584=CARTESIAN_POINT('Ctrl Pts',(23.2817506471191,-3.81885747554393,331.897764952859));
#66585=CARTESIAN_POINT('Ctrl Pts',(23.2740555381452,-3.90134557327747,332.005223584244));
#66586=CARTESIAN_POINT('Ctrl Pts',(23.2663725283596,-3.983703973169,332.11251325607));
#66587=CARTESIAN_POINT('Ctrl Pts',(23.258689518574,-4.06175171740237,332.223357390518));
#66588=CARTESIAN_POINT('Ctrl Pts',(23.2510065087884,-4.13516406474217,332.337369492369));
#66589=CARTESIAN_POINT('Ctrl Pts',(23.2433304517848,-4.2085099771733,332.45127841834));
#66590=CARTESIAN_POINT('Ctrl Pts',(23.2356543947813,-4.27722861842953,332.568349277977));
#66591=CARTESIAN_POINT('Ctrl Pts',(23.2279783377777,-4.34103612823051,332.688163414967));
#66592=CARTESIAN_POINT('Ctrl Pts',(23.2203074810163,-4.40480041082547,332.807896382352));
#66593=CARTESIAN_POINT('Ctrl Pts',(23.2126366242549,-4.46365999172824,332.9303685797));
#66594=CARTESIAN_POINT('Ctrl Pts',(23.2049657674934,-4.51737517144896,333.05513377764));
#66595=CARTESIAN_POINT('Ctrl Pts',(23.1972983628446,-4.57106617774835,333.179842827547));
#66596=CARTESIAN_POINT('Ctrl Pts',(23.1896309581957,-4.61961723109349,333.306842458638));
#66597=CARTESIAN_POINT('Ctrl Pts',(23.181963553547,-4.66283554291853,333.435663795025));
#66598=CARTESIAN_POINT('Ctrl Pts',(23.1742958932823,-4.70605529555513,333.564489426056));
#66599=CARTESIAN_POINT('Ctrl Pts',(23.1666282330176,-4.74394181174648,333.695136509071));
#66600=CARTESIAN_POINT('Ctrl Pts',(23.158960572753,-4.77635129521544,333.827118349025));
#66601=CARTESIAN_POINT('Ctrl Pts',(23.1512931116582,-4.8087599368379,333.95909676071));
#66602=CARTESIAN_POINT('Ctrl Pts',(23.1436256505635,-4.83569173914186,334.092409470559));
#66603=CARTESIAN_POINT('Ctrl Pts',(23.1359581894687,-4.85705365503044,334.226557788419));
#66604=CARTESIAN_POINT('Ctrl Pts',(23.1282854233609,-4.87843035094071,334.360798921691));
#66605=CARTESIAN_POINT('Ctrl Pts',(23.1206126572532,-4.89422940212695,334.495876422066));
#66606=CARTESIAN_POINT('Ctrl Pts',(23.1129398911455,-4.90440943298956,334.63128442384));
#66607=CARTESIAN_POINT('Ctrl Pts',(23.1058990529332,-4.91375103799781,334.755540242373));
#66608=CARTESIAN_POINT('Ctrl Pts',(23.098858214721,-4.91836165408909,334.880074063817));
#66609=CARTESIAN_POINT('Ctrl Pts',(23.0918173765087,-4.91824794611184,335.004494782163));
#66610=CARTESIAN_POINT('',(21.3418173764747,-4.91824992891069,334.999163776336));
#66611=CARTESIAN_POINT('Ctrl Pts',(23.0918173764689,-4.91824794611119,335.004494782867));
#66612=CARTESIAN_POINT('Ctrl Pts',(23.0820354501074,-4.91808997014287,335.177354074335));
#66613=CARTESIAN_POINT('Ctrl Pts',(23.0722535237459,-4.90881535265375,335.349806614891));
#66614=CARTESIAN_POINT('Ctrl Pts',(23.0624715973843,-4.89057380172721,335.521028744274));
#66615=CARTESIAN_POINT('Ctrl Pts',(23.0524996235227,-4.87197784605229,335.69557745131));
#66616=CARTESIAN_POINT('Ctrl Pts',(23.0425276496611,-4.84406315992271,335.868847655051));
#66617=CARTESIAN_POINT('Ctrl Pts',(23.0325556757995,-4.80703664690709,336.039991220055));
#66618=CARTESIAN_POINT('Ctrl Pts',(23.028004727464,-4.79013871374812,336.118096671703));
#66619=CARTESIAN_POINT('Ctrl Pts',(23.0234537791286,-4.77134364998109,336.195759508206));
#66620=CARTESIAN_POINT('Ctrl Pts',(23.0189028307932,-4.75067438848183,336.272900592003));
#66621=CARTESIAN_POINT('Ctrl Pts',(23.0111277520147,-4.71536193828395,336.404692464679));
#66622=CARTESIAN_POINT('Ctrl Pts',(23.0033526732363,-4.67450533258638,336.535222038394));
#66623=CARTESIAN_POINT('Ctrl Pts',(22.9955775944578,-4.62821014747037,336.663987347714));
#66624=CARTESIAN_POINT('Ctrl Pts',(22.9878120834088,-4.58197193152694,336.792594203123));
#66625=CARTESIAN_POINT('Ctrl Pts',(22.9800465723598,-4.53030858333734,336.919440749576));
#66626=CARTESIAN_POINT('Ctrl Pts',(22.9722810613108,-4.47337620732547,337.044037272222));
#66627=CARTESIAN_POINT('Ctrl Pts',(22.9645232497886,-4.41650027993013,337.168510257054));
#66628=CARTESIAN_POINT('Ctrl Pts',(22.9567654382663,-4.3543658826801,337.290737304477));
#66629=CARTESIAN_POINT('Ctrl Pts',(22.9490076267441,-4.287178119855,337.410246217949));
#66630=CARTESIAN_POINT('Ctrl Pts',(22.9412556532211,-4.22004091795226,337.529665197173));
#66631=CARTESIAN_POINT('Ctrl Pts',(22.9335036796981,-4.14785811057876,337.646369774528));
#66632=CARTESIAN_POINT('Ctrl Pts',(22.9257517061751,-4.07088171624043,337.759910345442));
#66633=CARTESIAN_POINT('Ctrl Pts',(22.9180030156175,-3.99393792145069,337.873402831858));
#66634=CARTESIAN_POINT('Ctrl Pts',(22.9102543250599,-3.91220479628132,337.983733654058));
#66635=CARTESIAN_POINT('Ctrl Pts',(22.9025056345023,-3.82597873719878,338.090480507138));
#66636=CARTESIAN_POINT('Ctrl Pts',(22.8947585561245,-3.73977061816789,338.197205150644));
#66637=CARTESIAN_POINT('Ctrl Pts',(22.8870114777466,-3.64907167005151,338.300347004353));
#66638=CARTESIAN_POINT('Ctrl Pts',(22.8792643993688,-3.55421954813177,338.399515622288));
#66639=CARTESIAN_POINT('Ctrl Pts',(22.871517256063,-3.45936663126001,338.498685071351));
#66640=CARTESIAN_POINT('Ctrl Pts',(22.8637701127571,-3.36036074133253,338.593880935752));
#66641=CARTESIAN_POINT('Ctrl Pts',(22.8560229694513,-3.25757719608487,338.684748821025));
#66642=CARTESIAN_POINT('Ctrl Pts',(22.8482740844232,-3.15477054291421,338.775637135329));
#66643=CARTESIAN_POINT('Ctrl Pts',(22.8405251993951,-3.04818483720247,338.862195275458));
#66644=CARTESIAN_POINT('Ctrl Pts',(22.832776314367,-2.93822902802969,338.944108675144));
#66645=CARTESIAN_POINT('Ctrl Pts',(22.8250192045923,-2.82815651062484,339.026109018559));
#66646=CARTESIAN_POINT('Ctrl Pts',(22.8172620948176,-2.71470705819097,339.103454539559));
#66647=CARTESIAN_POINT('Ctrl Pts',(22.8095049850429,-2.59831965715527,339.175873324437));
#66648=CARTESIAN_POINT('Ctrl Pts',(22.8017437301167,-2.48187006241388,339.248330807597));
#66649=CARTESIAN_POINT('Ctrl Pts',(22.7939824751905,-2.3624797308668,339.315856116431));
#66650=CARTESIAN_POINT('Ctrl Pts',(22.7862212202643,-2.24061199712329,339.378223491423));
#66651=CARTESIAN_POINT('Ctrl Pts',(22.7784475498597,-2.11854931472239,339.440690633889));
#66652=CARTESIAN_POINT('Ctrl Pts',(22.770673879455,-1.99400166609688,339.49798319111));
#66653=CARTESIAN_POINT('Ctrl Pts',(22.7629002090504,-1.86745291224435,339.549923371118));
#66654=CARTESIAN_POINT('Ctrl Pts',(22.7554884048733,-1.74679503333055,339.599445723252));
#66655=CARTESIAN_POINT('Ctrl Pts',(22.7480766006964,-1.62431842983969,339.644102691832));
#66656=CARTESIAN_POINT('Ctrl Pts',(22.7406647965193,-1.50045324128822,339.683782993821));
#66657=CARTESIAN_POINT('Ctrl Pts',(22.7328897177409,-1.3705170508693,339.725408145612));
#66658=CARTESIAN_POINT('Ctrl Pts',(22.7251146389625,-1.23864209391131,339.761687996366));
#66659=CARTESIAN_POINT('Ctrl Pts',(22.717339560184,-1.10530761713335,339.792439684963));
#66660=CARTESIAN_POINT('Ctrl Pts',(22.709574049135,-0.972137216917547,339.823153531649));
#66661=CARTESIAN_POINT('Ctrl Pts',(22.701808538086,-0.837511247705164,339.848352664706));
#66662=CARTESIAN_POINT('Ctrl Pts',(22.694043027037,-0.701925998222751,339.867903342869));
#66663=CARTESIAN_POINT('Ctrl Pts',(22.6862852155148,-0.566475181909853,
339.887434636479));
#66664=CARTESIAN_POINT('Ctrl Pts',(22.6785274039926,-0.430067362508664,
339.901328564999));
#66665=CARTESIAN_POINT('Ctrl Pts',(22.6707695924704,-0.293210613862012,
339.909502072351));
#66666=CARTESIAN_POINT('Ctrl Pts',(22.6630176189473,-0.156456854258879,
339.917669428879));
#66667=CARTESIAN_POINT('Ctrl Pts',(22.6552656454243,-0.0192552264593384,
339.92012490952));
#66668=CARTESIAN_POINT('Ctrl Pts',(22.6475136719013,0.117879805785627,339.91683713518));
#66669=CARTESIAN_POINT('Ctrl Pts',(22.6397649813437,0.254956761263019,339.913550753215));
#66670=CARTESIAN_POINT('Ctrl Pts',(22.6320162907861,0.391966787331368,339.904525963234));
#66671=CARTESIAN_POINT('Ctrl Pts',(22.6242676002285,0.528394361650382,339.889783477934));
#66672=CARTESIAN_POINT('Ctrl Pts',(22.6165205218506,0.66479355107328,339.875044059931));
#66673=CARTESIAN_POINT('Ctrl Pts',(22.6087734434728,0.800610141422339,339.854589354803));
#66674=CARTESIAN_POINT('Ctrl Pts',(22.6010263650949,0.935333073697483,339.828492011358));
#66675=CARTESIAN_POINT('Ctrl Pts',(22.5932792217891,1.07005713508019,339.802394449192));
#66676=CARTESIAN_POINT('Ctrl Pts',(22.5855320784833,1.20368713636607,339.770654228719));
#66677=CARTESIAN_POINT('Ctrl Pts',(22.5777849351775,1.33572195372598,339.733395179449));
#66678=CARTESIAN_POINT('Ctrl Pts',(22.5700360501494,1.4677864553162,339.696127753554));
#66679=CARTESIAN_POINT('Ctrl Pts',(22.5622871651213,1.59825468323484,339.653339136044));
#66680=CARTESIAN_POINT('Ctrl Pts',(22.5545382800932,1.72664080618307,339.605202991066));
#66681=CARTESIAN_POINT('Ctrl Pts',(22.5467811703185,1.85516319948868,339.557015753887));
#66682=CARTESIAN_POINT('Ctrl Pts',(22.5390240605438,1.98159870663285,339.503469788496));
#66683=CARTESIAN_POINT('Ctrl Pts',(22.531266950769,2.10548110883107,339.444787099835));
#66684=CARTESIAN_POINT('Ctrl Pts',(22.5235056958429,2.22942970982394,339.386073053021));
#66685=CARTESIAN_POINT('Ctrl Pts',(22.5157444409167,2.35082214162788,339.322216995354));
#66686=CARTESIAN_POINT('Ctrl Pts',(22.5079831859905,2.46921782130587,339.253486383362));
#66687=CARTESIAN_POINT('Ctrl Pts',(22.5002095155858,2.58780289548628,339.18464582479));
#66688=CARTESIAN_POINT('Ctrl Pts',(22.4924358451811,2.7033813083497,339.110915340112));
#66689=CARTESIAN_POINT('Ctrl Pts',(22.4846621747765,2.81554170588994,339.032605604928));
#66690=CARTESIAN_POINT('Ctrl Pts',(22.4772503705994,2.92248100994075,338.957941206756));
#66691=CARTESIAN_POINT('Ctrl Pts',(22.4698385664223,3.02631312539106,338.879114466072));
#66692=CARTESIAN_POINT('Ctrl Pts',(22.4624267622451,3.12671169878485,338.796426874731));
#66693=CARTESIAN_POINT('Ctrl Pts',(22.4546516834667,3.23203110533235,338.709686518226));
#66694=CARTESIAN_POINT('Ctrl Pts',(22.4468766046883,3.33390471202152,338.618423162471));
#66695=CARTESIAN_POINT('Ctrl Pts',(22.4391015259098,3.43191939913591,338.522940859614));
#66696=CARTESIAN_POINT('Ctrl Pts',(22.4313360148608,3.52981347293789,338.427576053808));
#66697=CARTESIAN_POINT('Ctrl Pts',(22.4235705038118,3.62385779830284,338.328002901001));
#66698=CARTESIAN_POINT('Ctrl Pts',(22.4158049927628,3.71367133904075,338.224566365899));
#66699=CARTESIAN_POINT('Ctrl Pts',(22.4080471812406,3.80339582939158,338.121232388422));
#66700=CARTESIAN_POINT('Ctrl Pts',(22.4002893697184,3.88889762845553,338.014042944911));
#66701=CARTESIAN_POINT('Ctrl Pts',(22.3925315581962,3.96983194469297,337.903380339087));
#66702=CARTESIAN_POINT('Ctrl Pts',(22.3847795846732,4.05070535529075,337.792801010383));
#66703=CARTESIAN_POINT('Ctrl Pts',(22.3770276111501,4.12701789477725,337.678754035968));
#66704=CARTESIAN_POINT('Ctrl Pts',(22.3692756376271,4.19846476994724,337.561655058358));
#66705=CARTESIAN_POINT('Ctrl Pts',(22.3615269470695,4.26988138732318,337.444605672234));
#66706=CARTESIAN_POINT('Ctrl Pts',(22.3537782565119,4.33643623563221,337.324507186632));
#66707=CARTESIAN_POINT('Ctrl Pts',(22.3460295659543,4.39786775390278,337.201804324113));
#66708=CARTESIAN_POINT('Ctrl Pts',(22.3382824875764,4.45928649083288,337.079126990949));
#66709=CARTESIAN_POINT('Ctrl Pts',(22.3305354091986,4.51558384310076,336.953846707969));
#66710=CARTESIAN_POINT('Ctrl Pts',(22.3227883308208,4.56654433928952,336.826432550028));
#66711=CARTESIAN_POINT('Ctrl Pts',(22.315041187515,4.61750526257631,336.699017324234));
#66712=CARTESIAN_POINT('Ctrl Pts',(22.3072940442091,4.66312909541628,336.56946855073));
#66713=CARTESIAN_POINT('Ctrl Pts',(22.2995469009033,4.70324878182811,336.438274646489));
#66714=CARTESIAN_POINT('Ctrl Pts',(22.2917980158752,4.74337748799716,336.307051247073));
#66715=CARTESIAN_POINT('Ctrl Pts',(22.2840491308471,4.77799947106941,336.174182354653));
#66716=CARTESIAN_POINT('Ctrl Pts',(22.276300245819,4.80699785773934,336.04017049477));
#66717=CARTESIAN_POINT('Ctrl Pts',(22.2685431360443,4.83602702359653,335.906016393313));
#66718=CARTESIAN_POINT('Ctrl Pts',(22.2607860262696,4.85942058672978,335.770717283632));
#66719=CARTESIAN_POINT('Ctrl Pts',(22.2530289164948,4.87711293809443,335.634785358662));
#66720=CARTESIAN_POINT('Ctrl Pts',(22.2452676615687,4.89481474368594,335.498780796018));
#66721=CARTESIAN_POINT('Ctrl Pts',(22.2375064066425,4.90680923282958,335.362143133456));
#66722=CARTESIAN_POINT('Ctrl Pts',(22.2297451517163,4.91308289071888,335.225387602644));
#66723=CARTESIAN_POINT('Ctrl Pts',(22.2219714813117,4.91936658441621,335.08841330755));
#66724=CARTESIAN_POINT('Ctrl Pts',(22.214197810907,4.91991115796733,334.951321158502));
#66725=CARTESIAN_POINT('Ctrl Pts',(22.2064241405023,4.9147552578573,334.814625196254));
#66726=CARTESIAN_POINT('Ctrl Pts',(22.1990123363253,4.90983936613787,334.684292463936));
#66727=CARTESIAN_POINT('Ctrl Pts',(22.1916005321483,4.89974179375709,334.554320150432));
#66728=CARTESIAN_POINT('Ctrl Pts',(22.1841887279713,4.884539463069,334.42514584787));
#66729=CARTESIAN_POINT('Ctrl Pts',(22.1764136491928,4.86859202086835,334.289640327947));
#66730=CARTESIAN_POINT('Ctrl Pts',(22.1686385704144,4.84697637208206,334.154584800215));
#66731=CARTESIAN_POINT('Ctrl Pts',(22.160863491636,4.81972463786244,334.020491205919));
#66732=CARTESIAN_POINT('Ctrl Pts',(22.1530979805869,4.79250643863674,333.886562622328));
#66733=CARTESIAN_POINT('Ctrl Pts',(22.1453324695379,4.7596660308589,333.753593996291));
#66734=CARTESIAN_POINT('Ctrl Pts',(22.1375669584889,4.7212873021629,333.622092429466));
#66735=CARTESIAN_POINT('Ctrl Pts',(22.1298091469667,4.68294662608811,333.490721246827));
#66736=CARTESIAN_POINT('Ctrl Pts',(22.1220513354445,4.63907866581843,333.36081460148));
#66737=CARTESIAN_POINT('Ctrl Pts',(22.1142935239223,4.58981832222422,333.232869322468));
#66738=CARTESIAN_POINT('Ctrl Pts',(22.1065415503993,4.54059504860078,333.105020326336));
#66739=CARTESIAN_POINT('Ctrl Pts',(22.0987895768763,4.48598760865884,332.979130121955));
#66740=CARTESIAN_POINT('Ctrl Pts',(22.0910376033533,4.42618058396466,332.85567994445));
#66741=CARTESIAN_POINT('Ctrl Pts',(22.0832889127956,4.36639888758086,332.732282048168));
#66742=CARTESIAN_POINT('Ctrl Pts',(22.0755402222381,4.30142215618538,332.61132247453));
#66743=CARTESIAN_POINT('Ctrl Pts',(22.0677915316805,4.23148282081839,332.493261840635));
#66744=CARTESIAN_POINT('Ctrl Pts',(22.0600444533026,4.16155803691427,332.37522577024));
#66745=CARTESIAN_POINT('Ctrl Pts',(22.0522973749248,4.08667290187253,332.260087775965));
#66746=CARTESIAN_POINT('Ctrl Pts',(22.0445502965469,4.00710526679841,332.148282895641));
#66747=CARTESIAN_POINT('Ctrl Pts',(22.0368031532411,3.92753696487097,332.036477078284));
#66748=CARTESIAN_POINT('Ctrl Pts',(22.0290560099353,3.84328631127445,331.928004749057));
#66749=CARTESIAN_POINT('Ctrl Pts',(22.0213088666295,3.75467362268367,331.823270699348));
#66750=CARTESIAN_POINT('Ctrl Pts',(22.0135599816014,3.6660410120792,331.718513103201));
#66751=CARTESIAN_POINT('Ctrl Pts',(22.0058110965733,3.57304466745953,331.617495757304));
#66752=CARTESIAN_POINT('Ctrl Pts',(21.9980622115452,3.47604392641988,331.520588888318));
#66753=CARTESIAN_POINT('Ctrl Pts',(21.9903051017705,3.37894022779148,331.423579161379));
#66754=CARTESIAN_POINT('Ctrl Pts',(21.9825479919958,3.27782391931504,331.330688903351));
#66755=CARTESIAN_POINT('Ctrl Pts',(21.9747908822211,3.17309021013766,331.242250463265));
#66756=CARTESIAN_POINT('Ctrl Pts',(21.9670296272949,3.06830053461491,331.153764764505));
#66757=CARTESIAN_POINT('Ctrl Pts',(21.9592683723687,2.95988991544971,331.069735863214));
#66758=CARTESIAN_POINT('Ctrl Pts',(21.9515071174426,2.84828430830456,330.990453945698));
#66759=CARTESIAN_POINT('Ctrl Pts',(21.9437334470379,2.73650016856,330.911045202953));
#66760=CARTESIAN_POINT('Ctrl Pts',(21.9359597766333,2.6215111556889,330.83639883124));
#66761=CARTESIAN_POINT('Ctrl Pts',(21.9281861062286,2.50377045135867,330.766760508853));
#66762=CARTESIAN_POINT('Ctrl Pts',(21.9207743020515,2.39151060514179,330.700363867128));
#66763=CARTESIAN_POINT('Ctrl Pts',(21.9133624978744,2.27674973806406,330.638519654518));
#66764=CARTESIAN_POINT('Ctrl Pts',(21.9059506936973,2.15989745778063,330.581399991584));
#66765=CARTESIAN_POINT('Ctrl Pts',(21.8981756149189,2.03731789915562,330.521480723819));
#66766=CARTESIAN_POINT('Ctrl Pts',(21.8904005361405,1.91204935673871,330.466571488493));
#66767=CARTESIAN_POINT('Ctrl Pts',(21.8826254573621,1.7845397154436,330.416922315026));
#66768=CARTESIAN_POINT('Ctrl Pts',(21.874859946313,1.65718698287976,330.367334238028));
#66769=CARTESIAN_POINT('Ctrl Pts',(21.8670944352641,1.52759899945329,330.322993484261));
#66770=CARTESIAN_POINT('Ctrl Pts',(21.859328924215,1.39624759417864,330.284103932628));
#66771=CARTESIAN_POINT('Ctrl Pts',(21.8515711126929,1.26502642420484,330.245252940099));
#66772=CARTESIAN_POINT('Ctrl Pts',(21.8438133011707,1.1320456842512,330.211842503933));
#66773=CARTESIAN_POINT('Ctrl Pts',(21.8360554896485,0.997796171060482,330.184028045813));
#66774=CARTESIAN_POINT('Ctrl Pts',(21.8283035161255,0.863647684885555,330.156234518954));
#66775=CARTESIAN_POINT('Ctrl Pts',(21.8205515426025,0.728232707145237,330.134028667031));
#66776=CARTESIAN_POINT('Ctrl Pts',(21.8127995690795,0.592055806398295,330.117515695406));
#66777=CARTESIAN_POINT('Ctrl Pts',(21.8050508785219,0.455936576649853,330.101009717033));
#66778=CARTESIAN_POINT('Ctrl Pts',(21.7973021879642,0.3190564528966,330.090191870727));
#66779=CARTESIAN_POINT('Ctrl Pts',(21.7895534974066,0.181928559655519,330.085115966609));
#66780=CARTESIAN_POINT('Ctrl Pts',(21.7818064190288,0.0448291970179419,
330.080041118575));
#66781=CARTESIAN_POINT('Ctrl Pts',(21.774059340651,-0.0925174422083032,
330.080705850917));
#66782=CARTESIAN_POINT('Ctrl Pts',(21.7663122622732,-0.229595164254071,
330.087111936645));
#66783=CARTESIAN_POINT('Ctrl Pts',(21.7585651189674,-0.366674035142992,
330.093518076063));
#66784=CARTESIAN_POINT('Ctrl Pts',(21.7508179756615,-0.50348359390794,330.105665646596));
#66785=CARTESIAN_POINT('Ctrl Pts',(21.7430708323558,-0.639510101102596,
330.123504342964));
#66786=CARTESIAN_POINT('Ctrl Pts',(21.7353219473277,-0.77556718994418,330.141347049851));
#66787=CARTESIAN_POINT('Ctrl Pts',(21.7275730622996,-0.910840489422211,
330.164883377792));
#66788=CARTESIAN_POINT('Ctrl Pts',(21.7198241772715,-1.04482420984807,330.194011503029));
#66789=CARTESIAN_POINT('Ctrl Pts',(21.7120670674968,-1.1789501419791,330.223170545159));
#66790=CARTESIAN_POINT('Ctrl Pts',(21.704309957722,-1.31178337825074,330.257933157518));
#66791=CARTESIAN_POINT('Ctrl Pts',(21.6965528479473,-1.44283056892518,330.298146853434));
#66792=CARTESIAN_POINT('Ctrl Pts',(21.6887915930212,-1.57394778702816,330.338382038263));
#66793=CARTESIAN_POINT('Ctrl Pts',(21.681030338095,-1.70327668943253,330.384073980692));
#66794=CARTESIAN_POINT('Ctrl Pts',(21.6732690831689,-1.83034274323121,330.435021521978));
#66795=CARTESIAN_POINT('Ctrl Pts',(21.6654954127642,-1.95761206130524,330.486050562727));
#66796=CARTESIAN_POINT('Ctrl Pts',(21.6577217423596,-2.08261094072176,330.542351841892));
#66797=CARTESIAN_POINT('Ctrl Pts',(21.6499480719549,-2.20488754275825,330.603677219961));
#66798=CARTESIAN_POINT('Ctrl Pts',(21.6425362677778,-2.32147213955305,330.662147886928));
#66799=CARTESIAN_POINT('Ctrl Pts',(21.6351244636006,-2.4355819474791,330.725185296306));
#66800=CARTESIAN_POINT('Ctrl Pts',(21.6277126594235,-2.54685056447943,330.792538144592));
#66801=CARTESIAN_POINT('Ctrl Pts',(21.619937580645,-2.66357278785013,330.863192156606));
#66802=CARTESIAN_POINT('Ctrl Pts',(21.6121625018666,-2.7775371314825,330.938818608485));
#66803=CARTESIAN_POINT('Ctrl Pts',(21.6043874230882,-2.88829096407598,331.019176169518));
#66804=CARTESIAN_POINT('Ctrl Pts',(21.5966219120391,-2.99890850702751,331.099434845455));
#66805=CARTESIAN_POINT('Ctrl Pts',(21.5888564009901,-3.10632308642778,331.184412819222));
#66806=CARTESIAN_POINT('Ctrl Pts',(21.5810908899411,-3.2101079224042,331.273823650306));
#66807=CARTESIAN_POINT('Ctrl Pts',(21.5733330784189,-3.31378985541352,331.363145830291));
#66808=CARTESIAN_POINT('Ctrl Pts',(21.5655752668967,-3.41384891278834,331.456891867438));
#66809=CARTESIAN_POINT('Ctrl Pts',(21.5578174553745,-3.50988879884018,331.554733147886));
#66810=CARTESIAN_POINT('Ctrl Pts',(21.5500654818515,-3.60585641183216,331.652500799667));
#66811=CARTESIAN_POINT('Ctrl Pts',(21.5423135083285,-3.69781060102026,331.754357282754));
#66812=CARTESIAN_POINT('Ctrl Pts',(21.5345615348055,-3.78538984597211,331.859935227338));
#66813=CARTESIAN_POINT('Ctrl Pts',(21.5268128442478,-3.87293200106186,331.9654684596));
#66814=CARTESIAN_POINT('Ctrl Pts',(21.5190641536902,-3.9561026479521,332.07471971851));
#66815=CARTESIAN_POINT('Ctrl Pts',(21.5113154631325,-4.03457885544455,332.187286626458));
#66816=CARTESIAN_POINT('Ctrl Pts',(21.5035683847547,-4.1130387353066,332.299830113921));
#66817=CARTESIAN_POINT('Ctrl Pts',(21.4958213063768,-4.18680589513273,332.415687557822));
#66818=CARTESIAN_POINT('Ctrl Pts',(21.488074227999,-4.25559950189281,332.534425839284));
#66819=CARTESIAN_POINT('Ctrl Pts',(21.4803270846931,-4.32439368520948,332.653165115888));
#66820=CARTESIAN_POINT('Ctrl Pts',(21.4725799413874,-4.38821403637023,332.77478494));
#66821=CARTESIAN_POINT('Ctrl Pts',(21.4648327980815,-4.44682484426436,332.898826074088));
#66822=CARTESIAN_POINT('Ctrl Pts',(21.4570839130534,-4.50544882911236,333.022895095256));
#66823=CARTESIAN_POINT('Ctrl Pts',(21.4493350280254,-4.55886077314829,333.14938615628));
#66824=CARTESIAN_POINT('Ctrl Pts',(21.4415861429973,-4.6068725903219,333.27781882514));
#66825=CARTESIAN_POINT('Ctrl Pts',(21.4338290332226,-4.65493536773438,333.406387813763));
#66826=CARTESIAN_POINT('Ctrl Pts',(21.4260719234478,-4.69758643149004,333.536902160242));
#66827=CARTESIAN_POINT('Ctrl Pts',(21.418314813673,-4.7346870310329,333.668864476971));
#66828=CARTESIAN_POINT('Ctrl Pts',(21.4105535587469,-4.77180745594989,333.800897310143));
#66829=CARTESIAN_POINT('Ctrl Pts',(21.4027923038207,-4.80337141674832,333.934379275138));
#66830=CARTESIAN_POINT('Ctrl Pts',(21.3950310488945,-4.82929127512125,334.068802468572));
#66831=CARTESIAN_POINT('Ctrl Pts',(21.3872573784899,-4.85525259682032,334.203440695307));
#66832=CARTESIAN_POINT('Ctrl Pts',(21.3794837080852,-4.87555171612219,334.339022772466));
#66833=CARTESIAN_POINT('Ctrl Pts',(21.3717100376805,-4.89015278297577,334.475034456698));
#66834=CARTESIAN_POINT('Ctrl Pts',(21.3642982335035,-4.90407416665439,334.604714764306));
#66835=CARTESIAN_POINT('Ctrl Pts',(21.3568864293264,-4.91281602895181,334.734785295515));
#66836=CARTESIAN_POINT('Ctrl Pts',(21.3494746251494,-4.91639141516887,334.864801940273));
#66837=CARTESIAN_POINT('Ctrl Pts',(21.3469222089359,-4.9176226772924,334.909576003941));
#66838=CARTESIAN_POINT('Ctrl Pts',(21.3443697927223,-4.91824231234348,334.954366964292));
#66839=CARTESIAN_POINT('Ctrl Pts',(21.3418173765088,-4.91824992891059,334.999163775737));
#66840=CARTESIAN_POINT('',(19.591817376556,-4.91824833437501,334.995952294795));
#66841=CARTESIAN_POINT('Ctrl Pts',(21.3418173764747,-4.91824992891069,334.999163776336));
#66842=CARTESIAN_POINT('Ctrl Pts',(21.3340781614017,-4.91827302318835,335.134992782795));
#66843=CARTESIAN_POINT('Ctrl Pts',(21.3263389463286,-4.91266500023186,335.271045543282));
#66844=CARTESIAN_POINT('Ctrl Pts',(21.3185997312556,-4.90139628266234,335.406813892098));
#66845=CARTESIAN_POINT('Ctrl Pts',(21.3108699817983,-4.89014134754353,335.542416186475));
#66846=CARTESIAN_POINT('Ctrl Pts',(21.3031402323411,-4.87323952338996,335.677734371529));
#66847=CARTESIAN_POINT('Ctrl Pts',(21.2954104828838,-4.85071320889987,335.812258842675));
#66848=CARTESIAN_POINT('Ctrl Pts',(21.2876882948886,-4.82820893029523,335.946651718135));
#66849=CARTESIAN_POINT('Ctrl Pts',(21.2799661068934,-4.80009117369241,336.080252037651));
#66850=CARTESIAN_POINT('Ctrl Pts',(21.2722439188982,-4.76643421685168,336.212554295248));
#66851=CARTESIAN_POINT('Ctrl Pts',(21.2645273951655,-4.73280194755231,336.344759508497));
#66852=CARTESIAN_POINT('Ctrl Pts',(21.2568108714327,-4.69363866102598,336.475668173544));
#66853=CARTESIAN_POINT('Ctrl Pts',(21.2490943476999,-4.64906981683823,336.604784378246));
#66854=CARTESIAN_POINT('Ctrl Pts',(21.2413808473697,-4.60451843511945,336.733849994073));
#66855=CARTESIAN_POINT('Ctrl Pts',(21.2336673470394,-4.55456583540986,336.861124173388));
#66856=CARTESIAN_POINT('Ctrl Pts',(21.2259538467092,-4.49938742338047,336.98612584617));
#66857=CARTESIAN_POINT('Ctrl Pts',(21.218241735535,-4.44421894865832,337.111105006887));
#66858=CARTESIAN_POINT('Ctrl Pts',(21.2105296243608,-4.38382669268926,337.233812113929));
#66859=CARTESIAN_POINT('Ctrl Pts',(21.2028175131865,-4.31843415111682,337.353786214797));
#66860=CARTESIAN_POINT('Ctrl Pts',(21.195105081932,-4.2530388955193,337.47376529502));
#66861=CARTESIAN_POINT('Ctrl Pts',(21.1873926506776,-4.18264313041195,337.591010796669));
#66862=CARTESIAN_POINT('Ctrl Pts',(21.1796802194231,-4.10751602150002,337.705086910918));
#66863=CARTESIAN_POINT('Ctrl Pts',(21.1719657589653,-4.03236914603591,337.819193039519));
#66864=CARTESIAN_POINT('Ctrl Pts',(21.1642512985076,-3.95248866740103,337.93012779214));
#66865=CARTESIAN_POINT('Ctrl Pts',(21.1565368380498,-3.86818646389571,338.037485233385));
#66866=CARTESIAN_POINT('Ctrl Pts',(21.1488141124454,-3.78379394038932,338.144957695636));
#66867=CARTESIAN_POINT('Ctrl Pts',(21.1410913868409,-3.69497047589397,338.248844881976));
#66868=CARTESIAN_POINT('Ctrl Pts',(21.1333686612365,-3.60206783149632,338.348774462367));
#66869=CARTESIAN_POINT('Ctrl Pts',(21.1256414708774,-3.5091114771092,338.448761815243));
#66870=CARTESIAN_POINT('Ctrl Pts',(21.1179142805183,-3.41207152574919,338.544786727556));
#66871=CARTESIAN_POINT('Ctrl Pts',(21.1101870901592,-3.31133500482889,338.636515302909));
#66872=CARTESIAN_POINT('Ctrl Pts',(21.1024481691868,-3.21044555624333,338.728383131006));
#66873=CARTESIAN_POINT('Ctrl Pts',(21.0947092482144,-3.10584863222559,338.815941342409));
#66874=CARTESIAN_POINT('Ctrl Pts',(21.0869703272419,-2.99796307032023,338.898897343031));
#66875=CARTESIAN_POINT('Ctrl Pts',(21.0817257484532,-2.92485025115604,338.955115681843));
#66876=CARTESIAN_POINT('Ctrl Pts',(21.0764811696644,-2.85022770775908,339.009221294894));
#66877=CARTESIAN_POINT('Ctrl Pts',(21.0712365908756,-2.77423242997752,339.061134999844));
#66878=CARTESIAN_POINT('Ctrl Pts',(21.0634615120971,-2.66156956507691,339.138096975616));
#66879=CARTESIAN_POINT('Ctrl Pts',(21.0556864333187,-2.54552365829148,339.210488821577));
#66880=CARTESIAN_POINT('Ctrl Pts',(21.0479113545403,-2.42650187869756,339.277998561848));
#66881=CARTESIAN_POINT('Ctrl Pts',(21.0401458434913,-2.30762656298088,339.345425227086));
#66882=CARTESIAN_POINT('Ctrl Pts',(21.0323803324422,-2.18578299752819,339.407981549316));
#66883=CARTESIAN_POINT('Ctrl Pts',(21.0246148213932,-2.0614086975397,339.465397769987));
#66884=CARTESIAN_POINT('Ctrl Pts',(21.0168570098711,-1.93715771503184,339.522757062309));
#66885=CARTESIAN_POINT('Ctrl Pts',(21.0090991983489,-1.81038134409719,339.574986232473));
#66886=CARTESIAN_POINT('Ctrl Pts',(21.0013413868267,-1.68154285413715,339.621860739161));
#66887=CARTESIAN_POINT('Ctrl Pts',(20.9935894133037,-1.5528013192265,339.668699971297));
#66888=CARTESIAN_POINT('Ctrl Pts',(20.9858374397807,-1.42200111993228,339.710192427485));
#66889=CARTESIAN_POINT('Ctrl Pts',(20.9780854662577,-1.28962639175671,339.746161273301));
#66890=CARTESIAN_POINT('Ctrl Pts',(20.9703367757001,-1.15730772435694,339.78211488629));
#66891=CARTESIAN_POINT('Ctrl Pts',(20.9625880851425,-1.02341623073437,339.812549439235));
#66892=CARTESIAN_POINT('Ctrl Pts',(20.9548393945848,-0.888451921028,339.837337723017));
#66893=CARTESIAN_POINT('Ctrl Pts',(20.947092316207,-0.753515691773504,339.86212084939));
#66894=CARTESIAN_POINT('Ctrl Pts',(20.9393452378292,-0.617507474614878,
339.881259972703));
#66895=CARTESIAN_POINT('Ctrl Pts',(20.9315981594513,-0.48093781743464,339.894678935156));
#66896=CARTESIAN_POINT('Ctrl Pts',(20.9238510161455,-0.344367015669321,
339.908098010073));
#66897=CARTESIAN_POINT('Ctrl Pts',(20.9161038728397,-0.2072351534981,339.915796790288));
#66898=CARTESIAN_POINT('Ctrl Pts',(20.9083567295339,-0.0700578565870874,
339.917751006225));
#66899=CARTESIAN_POINT('Ctrl Pts',(20.9006078445059,0.0671502806924412,
339.919705661512));
#66900=CARTESIAN_POINT('Ctrl Pts',(20.8928589594778,0.204403482279608,339.915913177015));
#66901=CARTESIAN_POINT('Ctrl Pts',(20.8851100744497,0.341186563463491,339.906401409527));
#66902=CARTESIAN_POINT('Ctrl Pts',(20.877352964675,0.478114827623163,339.896879546151));
#66903=CARTESIAN_POINT('Ctrl Pts',(20.8695958549003,0.614571584050395,339.881626300538));
#66904=CARTESIAN_POINT('Ctrl Pts',(20.8618387451255,0.750046655614415,339.86072145642));
#66905=CARTESIAN_POINT('Ctrl Pts',(20.8540774901994,0.885594120725117,339.839805441422));
#66906=CARTESIAN_POINT('Ctrl Pts',(20.8463162352732,1.02015847242363,339.81323188592));
#66907=CARTESIAN_POINT('Ctrl Pts',(20.8385549803471,1.15324113840553,339.781131449687));
#66908=CARTESIAN_POINT('Ctrl Pts',(20.8307813099424,1.28653669328146,339.748979663219));
#66909=CARTESIAN_POINT('Ctrl Pts',(20.8230076395377,1.41834545004566,339.711283436202));
#66910=CARTESIAN_POINT('Ctrl Pts',(20.815233969133,1.5481845218662,339.668223189689));
#66911=CARTESIAN_POINT('Ctrl Pts',(20.8078221649558,1.67197955365779,339.627167408011));
#66912=CARTESIAN_POINT('Ctrl Pts',(20.8004103607787,1.79398388203258,339.581235859985));
#66913=CARTESIAN_POINT('Ctrl Pts',(20.7929985566015,1.91379870860334,339.530624412313));
#66914=CARTESIAN_POINT('Ctrl Pts',(20.7852234778231,2.03948601673257,339.477532346828));
#66915=CARTESIAN_POINT('Ctrl Pts',(20.7774483990446,2.16316096328841,339.419122249775));
#66916=CARTESIAN_POINT('Ctrl Pts',(20.7696733202662,2.28434085854605,339.355567690265));
#66917=CARTESIAN_POINT('Ctrl Pts',(20.7619078092172,2.40537163422788,339.292091338686));
#66918=CARTESIAN_POINT('Ctrl Pts',(20.7541422981682,2.52391312482046,339.223483300518));
#66919=CARTESIAN_POINT('Ctrl Pts',(20.7463767871191,2.639501720024,339.149965509795));
#66920=CARTESIAN_POINT('Ctrl Pts',(20.7386189755969,2.75497570879895,339.076520612176));
#66921=CARTESIAN_POINT('Ctrl Pts',(20.7308611640747,2.86750230099026,338.998175858087));
#66922=CARTESIAN_POINT('Ctrl Pts',(20.7231033525525,2.97664197335678,338.915199308458));
#66923=CARTESIAN_POINT('Ctrl Pts',(20.7153513790295,3.08569951465867,338.832285201314));
#66924=CARTESIAN_POINT('Ctrl Pts',(20.7075994055065,3.19137489942236,338.744746472108));
#66925=CARTESIAN_POINT('Ctrl Pts',(20.6998474319835,3.29325743030678,338.652894545457));
#66926=CARTESIAN_POINT('Ctrl Pts',(20.6920987414259,3.39509681387887,338.561081518151));
#66927=CARTESIAN_POINT('Ctrl Pts',(20.6843500508682,3.49314624863431,338.464959187647));
#66928=CARTESIAN_POINT('Ctrl Pts',(20.6766013603106,3.58702817753414,338.364879182984));
#66929=CARTESIAN_POINT('Ctrl Pts',(20.6688542819328,3.68089057351467,338.264820000801));
#66930=CARTESIAN_POINT('Ctrl Pts',(20.6611072035549,3.77058692107839,338.160805067211));
#66931=CARTESIAN_POINT('Ctrl Pts',(20.6533601251771,3.85577689075191,338.053222499466));
#66932=CARTESIAN_POINT('Ctrl Pts',(20.6456129818713,3.94096757439943,337.945639030075));
#66933=CARTESIAN_POINT('Ctrl Pts',(20.6378658385655,4.02165156217347,337.834488173324));
#66934=CARTESIAN_POINT('Ctrl Pts',(20.6301186952597,4.09752941063708,337.720190396179));
#66935=CARTESIAN_POINT('Ctrl Pts',(20.6223698102316,4.17342431805196,337.605866922467));
#66936=CARTESIAN_POINT('Ctrl Pts',(20.6146209252034,4.24451071989516,337.488395446109));
#66937=CARTESIAN_POINT('Ctrl Pts',(20.6068720401753,4.31053324553024,337.368224271829));
#66938=CARTESIAN_POINT('Ctrl Pts',(20.5991149304006,4.37662584815616,337.247925546623));
#66939=CARTESIAN_POINT('Ctrl Pts',(20.5913578206259,4.43764364929566,337.124921742533));
#66940=CARTESIAN_POINT('Ctrl Pts',(20.5836007108511,4.49337765467301,336.999685053949));
#66941=CARTESIAN_POINT('Ctrl Pts',(20.575839455925,4.54914144252061,336.874381442883));
#66942=CARTESIAN_POINT('Ctrl Pts',(20.5680782009988,4.59961566478131,336.746842933062));
#66943=CARTESIAN_POINT('Ctrl Pts',(20.5603169460726,4.64464038996505,336.617559492076));
#66944=CARTESIAN_POINT('Ctrl Pts',(20.552543275668,4.68973714003569,336.488069239717));
#66945=CARTESIAN_POINT('Ctrl Pts',(20.5447696052633,4.72936685999392,336.35682885269));
#66946=CARTESIAN_POINT('Ctrl Pts',(20.5369959348586,4.76341995197727,336.224342037016));
#66947=CARTESIAN_POINT('Ctrl Pts',(20.5295841306816,4.79588786433558,336.098022514488));
#66948=CARTESIAN_POINT('Ctrl Pts',(20.5221723265046,4.82328658838349,335.970570275725));
#66949=CARTESIAN_POINT('Ctrl Pts',(20.5147605223277,4.84556501991885,335.842426673509));
#66950=CARTESIAN_POINT('Ctrl Pts',(20.5069854435492,4.86893538374813,335.708002371626));
#66951=CARTESIAN_POINT('Ctrl Pts',(20.4992103647708,4.88674469705931,335.572392415491));
#66952=CARTESIAN_POINT('Ctrl Pts',(20.4914352859923,4.89887770671504,335.436096637399));
#66953=CARTESIAN_POINT('Ctrl Pts',(20.4836697749433,4.91099578592995,335.299968579938));
#66954=CARTESIAN_POINT('Ctrl Pts',(20.4759042638943,4.91745142541496,335.163156765346));
#66955=CARTESIAN_POINT('Ctrl Pts',(20.4681387528453,4.91818036809998,335.026171154655));
#66956=CARTESIAN_POINT('Ctrl Pts',(20.4603809413231,4.9189085880362,334.889321365596));
#66957=CARTESIAN_POINT('Ctrl Pts',(20.4526231298009,4.91392140871967,334.752298511714));
#66958=CARTESIAN_POINT('Ctrl Pts',(20.4448653182787,4.90320639706054,334.615617260631));
#66959=CARTESIAN_POINT('Ctrl Pts',(20.4371133447557,4.89249944878744,334.479038866524));
#66960=CARTESIAN_POINT('Ctrl Pts',(20.4293613712326,4.87607327818888,334.342801951645));
#66961=CARTESIAN_POINT('Ctrl Pts',(20.4216093977096,4.85396751697297,334.207420409882));
#66962=CARTESIAN_POINT('Ctrl Pts',(20.413860707152,4.83187111756015,334.072096202283));
#66963=CARTESIAN_POINT('Ctrl Pts',(20.4061120165944,4.80409997438072,333.93762703227));
#66964=CARTESIAN_POINT('Ctrl Pts',(20.3983633260368,4.77074546201769,333.804520682263));
#66965=CARTESIAN_POINT('Ctrl Pts',(20.3906162476589,4.7373978893395,333.671442026143));
#66966=CARTESIAN_POINT('Ctrl Pts',(20.3828691692812,4.6984693530649,333.539726004948));
#66967=CARTESIAN_POINT('Ctrl Pts',(20.3751220909033,4.65410205746412,333.409868841508));
#66968=CARTESIAN_POINT('Ctrl Pts',(20.3673749475975,4.60973439002279,333.28001058974));
#66969=CARTESIAN_POINT('Ctrl Pts',(20.3596278042917,4.55992799871301,333.152011596681));
#66970=CARTESIAN_POINT('Ctrl Pts',(20.3518806609859,4.5048744171493,333.026351209507));
#66971=CARTESIAN_POINT('Ctrl Pts',(20.3441317759578,4.44980845837164,332.90066257121));
#66972=CARTESIAN_POINT('Ctrl Pts',(20.3363828909298,4.38949311873274,332.77731394297));
#66973=CARTESIAN_POINT('Ctrl Pts',(20.3286340059017,4.32416719153442,332.656762674811));
#66974=CARTESIAN_POINT('Ctrl Pts',(20.320876896127,4.25877192672194,332.536083452291));
#66975=CARTESIAN_POINT('Ctrl Pts',(20.3131197863522,4.18835563708923,332.418207865206));
#66976=CARTESIAN_POINT('Ctrl Pts',(20.3053626765775,4.11320230217769,332.303567192779));
#66977=CARTESIAN_POINT('Ctrl Pts',(20.2976014216514,4.03800880772707,332.188865260042));
#66978=CARTESIAN_POINT('Ctrl Pts',(20.2898401667252,3.95807345178008,332.0774020039));
#66979=CARTESIAN_POINT('Ctrl Pts',(20.2820789117991,3.87372171042888,331.969577063733));
#66980=CARTESIAN_POINT('Ctrl Pts',(20.2743052413944,3.78923503378156,331.861579638802));
#66981=CARTESIAN_POINT('Ctrl Pts',(20.2665315709897,3.70031810786214,331.757232457833));
#66982=CARTESIAN_POINT('Ctrl Pts',(20.258757900585,3.60733520011827,331.656900268241));
#66983=CARTESIAN_POINT('Ctrl Pts',(20.2513460964079,3.51868066909978,331.561238566212));
#66984=CARTESIAN_POINT('Ctrl Pts',(20.2439342922309,3.42633038416839,331.469226675029));
#66985=CARTESIAN_POINT('Ctrl Pts',(20.2365224880537,3.33062783287907,331.381146410622));
#66986=CARTESIAN_POINT('Ctrl Pts',(20.2287474092753,3.23023461446837,331.28874907008));
#66987=CARTESIAN_POINT('Ctrl Pts',(20.2209723304968,3.12583495057434,331.20038651001));
#66988=CARTESIAN_POINT('Ctrl Pts',(20.2131972517184,3.01778679075014,331.116426137168));
#66989=CARTESIAN_POINT('Ctrl Pts',(20.2054317406694,2.90987159106528,331.03256908291));
#66990=CARTESIAN_POINT('Ctrl Pts',(20.1976662296204,2.79831713437253,330.953103674806));
#66991=CARTESIAN_POINT('Ctrl Pts',(20.1899007185714,2.68351748459625,330.878359917173));
#66992=CARTESIAN_POINT('Ctrl Pts',(20.1821429070492,2.56883165900734,330.803690268194));
#66993=CARTESIAN_POINT('Ctrl Pts',(20.1743850955271,2.45090736903167,330.733733165073));
#66994=CARTESIAN_POINT('Ctrl Pts',(20.1666272840049,2.33017068139372,330.668777579242));
#66995=CARTESIAN_POINT('Ctrl Pts',(20.1588753104819,2.20952485194151,330.60387087455));
#66996=CARTESIAN_POINT('Ctrl Pts',(20.1511233369589,2.0860711802891,330.54395837993));
#66997=CARTESIAN_POINT('Ctrl Pts',(20.1433713634358,1.96026325776023,330.489284865703));
#66998=CARTESIAN_POINT('Ctrl Pts',(20.1356226728782,1.83450861496141,330.434634505742));
#66999=CARTESIAN_POINT('Ctrl Pts',(20.1278739823206,1.70640206204155,330.38521886878));
#67000=CARTESIAN_POINT('Ctrl Pts',(20.120125291763,1.57642005209949,330.341235906183));
#67001=CARTESIAN_POINT('Ctrl Pts',(20.1123782133851,1.44646508599987,330.297262094609));
#67002=CARTESIAN_POINT('Ctrl Pts',(20.1046311350074,1.31463580904178,330.258718834334));
#67003=CARTESIAN_POINT('Ctrl Pts',(20.0968840566295,1.18142646047917,330.225755077399));
#67004=CARTESIAN_POINT('Ctrl Pts',(20.0891369133238,1.04821599549483,330.192791044197));
#67005=CARTESIAN_POINT('Ctrl Pts',(20.0813897700179,0.913625815265672,330.165406701497));
#67006=CARTESIAN_POINT('Ctrl Pts',(20.0736426267122,0.778162662886691,330.143700386859));
#67007=CARTESIAN_POINT('Ctrl Pts',(20.065893741684,0.642669055513983,330.121989192181));
#67008=CARTESIAN_POINT('Ctrl Pts',(20.0581448566559,0.50630247132605,330.105958627571));
#67009=CARTESIAN_POINT('Ctrl Pts',(20.0503959716278,0.369576730474485,330.095655384989));
#67010=CARTESIAN_POINT('Ctrl Pts',(20.0426388618531,0.232705867509498,330.085341206438));
#67011=CARTESIAN_POINT('Ctrl Pts',(20.0348817520784,0.0954754767577634,
330.080766522784));
#67012=CARTESIAN_POINT('Ctrl Pts',(20.0271246423036,-0.0415980922557909,
330.081925919507));
#67013=CARTESIAN_POINT('Ctrl Pts',(20.0193633873775,-0.178744909002143,
330.083085935774));
#67014=CARTESIAN_POINT('Ctrl Pts',(20.0116021324513,-0.315734346848884,
330.089986118277));
#67015=CARTESIAN_POINT('Ctrl Pts',(20.0038408775251,-0.452054206727391,
330.102569035027));
#67016=CARTESIAN_POINT('Ctrl Pts',(19.9960672071205,-0.588592133954979,
330.115172080342));
#67017=CARTESIAN_POINT('Ctrl Pts',(19.9882935367158,-0.724457955247771,
330.133475973245));
#67018=CARTESIAN_POINT('Ctrl Pts',(19.9805198663111,-0.859147820708077,
330.157371779222));
#67019=CARTESIAN_POINT('Ctrl Pts',(19.973108062134,-0.987567840527064,330.180155229682));
#67020=CARTESIAN_POINT('Ctrl Pts',(19.9656962579569,-1.11491864104462,330.208021640528));
#67021=CARTESIAN_POINT('Ctrl Pts',(19.9582844537798,-1.24077735640801,330.240834672516));
#67022=CARTESIAN_POINT('Ctrl Pts',(19.9505093750013,-1.37280478232483,330.275255968947));
#67023=CARTESIAN_POINT('Ctrl Pts',(19.9427342962229,-1.50360739280519,330.315229822088));
#67024=CARTESIAN_POINT('Ctrl Pts',(19.9349592174445,-1.63268252062706,330.360654049401));
#67025=CARTESIAN_POINT('Ctrl Pts',(19.9271937063954,-1.76159881328716,330.40602237931));
#67026=CARTESIAN_POINT('Ctrl Pts',(19.9194281953464,-1.88879148779234,330.456827609804));
#67027=CARTESIAN_POINT('Ctrl Pts',(19.9116626842973,-2.01376978587077,330.512916948394));
#67028=CARTESIAN_POINT('Ctrl Pts',(19.9039048727751,-2.13862416760254,330.56895067424));
#67029=CARTESIAN_POINT('Ctrl Pts',(19.896147061253,-2.26126818788701,330.630257922849));
#67030=CARTESIAN_POINT('Ctrl Pts',(19.8883892497308,-2.38122827532967,330.696636784645));
#67031=CARTESIAN_POINT('Ctrl Pts',(19.8806372762077,-2.50109808900271,330.762965694243));
#67032=CARTESIAN_POINT('Ctrl Pts',(19.8728853026847,-2.61828764940724,330.834358431887));
#67033=CARTESIAN_POINT('Ctrl Pts',(19.8651333291616,-2.73234565966671,330.910566022223));
#67034=CARTESIAN_POINT('Ctrl Pts',(19.857384638604,-2.84635536629051,330.986741338598));
#67035=CARTESIAN_POINT('Ctrl Pts',(19.8496359480464,-2.95723583618581,331.067727235353));
#67036=CARTESIAN_POINT('Ctrl Pts',(19.8418872574888,-3.06456277171435,331.153230175755));
#67037=CARTESIAN_POINT('Ctrl Pts',(19.8341401791109,-3.17186737697768,331.238715326556));
#67038=CARTESIAN_POINT('Ctrl Pts',(19.8263931007331,-3.2756196129515,331.328715408258));
#67039=CARTESIAN_POINT('Ctrl Pts',(19.8186460223553,-3.37542676146652,331.422895411024));
#67040=CARTESIAN_POINT('Ctrl Pts',(19.8108988790495,-3.47523474646131,331.517076203108));
#67041=CARTESIAN_POINT('Ctrl Pts',(19.8031517357437,-3.57109729376166,331.615436717871));
#67042=CARTESIAN_POINT('Ctrl Pts',(19.7954045924379,-3.6626574814509,331.717604040328));
#67043=CARTESIAN_POINT('Ctrl Pts',(19.7876557074098,-3.75423825381433,331.819794332168));
#67044=CARTESIAN_POINT('Ctrl Pts',(19.7799068223817,-3.84151448100874,331.925792843721));
#67045=CARTESIAN_POINT('Ctrl Pts',(19.7721579373536,-3.9241688412019,332.035192760357));
#67046=CARTESIAN_POINT('Ctrl Pts',(19.7644008275789,-4.00691093158706,332.144708795195));
#67047=CARTESIAN_POINT('Ctrl Pts',(19.7566437178042,-4.08502111938218,332.25763313464));
#67048=CARTESIAN_POINT('Ctrl Pts',(19.7488866080294,-4.15822453141655,332.373528639253));
#67049=CARTESIAN_POINT('Ctrl Pts',(19.7411253531033,-4.23146706101377,332.489486074718));
#67050=CARTESIAN_POINT('Ctrl Pts',(19.7333640981771,-4.29979739560863,332.60841750023));
#67051=CARTESIAN_POINT('Ctrl Pts',(19.7256028432509,-4.36298665068126,332.729861116919));
#67052=CARTESIAN_POINT('Ctrl Pts',(19.7178291728463,-4.42627698796859,332.851499003816));
#67053=CARTESIAN_POINT('Ctrl Pts',(19.7100555024416,-4.48440964581031,332.975656758239));
#67054=CARTESIAN_POINT('Ctrl Pts',(19.7022818320369,-4.537203567473,333.101851731342));
#67055=CARTESIAN_POINT('Ctrl Pts',(19.6948700278599,-4.58753991938023,333.222172298085));
#67056=CARTESIAN_POINT('Ctrl Pts',(19.6874582236829,-4.63302328554313,333.344344417031));
#67057=CARTESIAN_POINT('Ctrl Pts',(19.6800464195059,-4.67353947956275,333.467938710277));
#67058=CARTESIAN_POINT('Ctrl Pts',(19.6707544085463,-4.72433371398656,333.622886075311));
#67059=CARTESIAN_POINT('Ctrl Pts',(19.6614623975868,-4.76745266189659,333.780466072888));
#67060=CARTESIAN_POINT('Ctrl Pts',(19.6521703866272,-4.80266013689503,333.939981758657));
#67061=CARTESIAN_POINT('Ctrl Pts',(19.6429295360595,-4.8376737649186,334.098619175447));
#67062=CARTESIAN_POINT('Ctrl Pts',(19.6336886854917,-4.86486272716904,334.259170985439));
#67063=CARTESIAN_POINT('Ctrl Pts',(19.6244478349239,-4.88404150409399,334.420930359294));
#67064=CARTESIAN_POINT('Ctrl Pts',(19.6152987034669,-4.90302992404358,334.581084207142));
#67065=CARTESIAN_POINT('Ctrl Pts',(19.6061495720097,-4.91416630650535,334.742421708532));
#67066=CARTESIAN_POINT('Ctrl Pts',(19.5970004405527,-4.91731760625495,334.904236636885));
#67067=CARTESIAN_POINT('Ctrl Pts',(19.5952727525538,-4.91791268599382,334.934793166876));
#67068=CARTESIAN_POINT('Ctrl Pts',(19.5935450645549,-4.91822316248318,334.965366664467));
#67069=CARTESIAN_POINT('Ctrl Pts',(19.591817376556,-4.91824833437501,334.995952294795));
#67070=CARTESIAN_POINT('',(17.841817376457,-4.91824925238431,335.002711811416));
#67071=CARTESIAN_POINT('Ctrl Pts',(19.5918173765088,-4.9182483343757,334.99595229563));
#67072=CARTESIAN_POINT('Ctrl Pts',(19.5839003352056,-4.91836368325021,335.136109371879));
#67073=CARTESIAN_POINT('Ctrl Pts',(19.5759832939023,-4.91248314281081,335.276354923141));
#67074=CARTESIAN_POINT('Ctrl Pts',(19.5680662525991,-4.90061363171136,335.416135909511));
#67075=CARTESIAN_POINT('Ctrl Pts',(19.5603456345828,-4.88903860541929,335.552448903266));
#67076=CARTESIAN_POINT('Ctrl Pts',(19.5526250165664,-4.8717683366803,335.688319701291));
#67077=CARTESIAN_POINT('Ctrl Pts',(19.5449043985501,-4.84886193943759,335.823238091182));
#67078=CARTESIAN_POINT('Ctrl Pts',(19.5371839329457,-4.82595599438794,335.958153817663));
#67079=CARTESIAN_POINT('Ctrl Pts',(19.5294634673413,-4.7974142076564,336.092116785396));
#67080=CARTESIAN_POINT('Ctrl Pts',(19.521743001737,-4.76334711911622,336.224625365288));
#67081=CARTESIAN_POINT('Ctrl Pts',(19.5140209910634,-4.72927321285147,336.357160463649));
#67082=CARTESIAN_POINT('Ctrl Pts',(19.5062989803899,-4.68967190260963,336.488240213965));
#67083=CARTESIAN_POINT('Ctrl Pts',(19.4985769697164,-4.64470394246313,336.617376996673));
#67084=CARTESIAN_POINT('Ctrl Pts',(19.4905129210093,-4.59774417560862,336.752233752207));
#67085=CARTESIAN_POINT('Ctrl Pts',(19.4824488723023,-4.54493159701169,336.884971021297));
#67086=CARTESIAN_POINT('Ctrl Pts',(19.4743848235953,-4.48650528533483,337.015056670956));
#67087=CARTESIAN_POINT('Ctrl Pts',(19.4666502342321,-4.43046599970475,337.139827628909));
#67088=CARTESIAN_POINT('Ctrl Pts',(19.4589156448689,-4.3692628586575,337.262159029399));
#67089=CARTESIAN_POINT('Ctrl Pts',(19.4511810555057,-4.30315346646788,337.381607294775));
#67090=CARTESIAN_POINT('Ctrl Pts',(19.4434408755016,-4.23699628972825,337.501141898588));
#67091=CARTESIAN_POINT('Ctrl Pts',(19.4357006954974,-4.16592600366716,337.617788882628));
#67092=CARTESIAN_POINT('Ctrl Pts',(19.4279605154933,-4.09024318364582,337.7311341529));
#67093=CARTESIAN_POINT('Ctrl Pts',(19.4202093897085,-4.0144533367149,337.844639710461));
#67094=CARTESIAN_POINT('Ctrl Pts',(19.4124582639238,-3.93403817053266,337.954833921385));
#67095=CARTESIAN_POINT('Ctrl Pts',(19.404707138139,-3.84933825326352,338.061335995029));
#67096=CARTESIAN_POINT('Ctrl Pts',(19.40374088717,-3.83877960934425,338.074612483467));
#67097=CARTESIAN_POINT('Ctrl Pts',(19.402774636201,-3.82815442665017,338.087831644003));
#67098=CARTESIAN_POINT('Ctrl Pts',(19.401808385232,-3.8174634036537,338.100992780428));
#67099=CARTESIAN_POINT('Ctrl Pts',(19.3940333064536,-3.73143653414728,338.206895776444));
#67100=CARTESIAN_POINT('Ctrl Pts',(19.3862582276751,-3.64086348977577,338.309383607315));
#67101=CARTESIAN_POINT('Ctrl Pts',(19.3784831488967,-3.54604552482822,338.408041108664));
#67102=CARTESIAN_POINT('Ctrl Pts',(19.3707176378477,-3.45134423942306,338.506577205677));
#67103=CARTESIAN_POINT('Ctrl Pts',(19.3629521267986,-3.35240869525998,338.601292072484));
#67104=CARTESIAN_POINT('Ctrl Pts',(19.3551866157496,-3.24958127500149,338.69180235111));
#67105=CARTESIAN_POINT('Ctrl Pts',(19.3474288042274,-3.14685580842964,338.78222288853));
#67106=CARTESIAN_POINT('Ctrl Pts',(19.3396709927052,-3.0402464365187,338.868446877444));
#67107=CARTESIAN_POINT('Ctrl Pts',(19.331913181183,-2.93013312495495,338.950126951446));
#67108=CARTESIAN_POINT('Ctrl Pts',(19.32416120766,-2.8201026771496,339.031745558603));
#67109=CARTESIAN_POINT('Ctrl Pts',(19.3164092341369,-2.70657385083344,339.108826825143));
#67110=CARTESIAN_POINT('Ctrl Pts',(19.3086572606139,-2.58996021994185,339.181063156856));
#67111=CARTESIAN_POINT('Ctrl Pts',(19.3009085700563,-2.47339597499264,339.253268896439));
#67112=CARTESIAN_POINT('Ctrl Pts',(19.2931598794986,-2.3537498554339,339.32063357674));
#67113=CARTESIAN_POINT('Ctrl Pts',(19.285411188941,-2.23146480664855,339.382892638337));
#67114=CARTESIAN_POINT('Ctrl Pts',(19.2776641105632,-2.10920520028877,339.445138746416));
#67115=CARTESIAN_POINT('Ctrl Pts',(19.2699170321853,-1.98430810491264,339.502281171483));
#67116=CARTESIAN_POINT('Ctrl Pts',(19.2621699538074,-1.85724112900778,339.554101278103));
#67117=CARTESIAN_POINT('Ctrl Pts',(19.2544228105016,-1.73017308815944,339.605921819026));
#67118=CARTESIAN_POINT('Ctrl Pts',(19.2466756671958,-1.60093549244348,339.652419804928));
#67119=CARTESIAN_POINT('Ctrl Pts',(19.23892852389,-1.47001561910445,339.693424884036));
#67120=CARTESIAN_POINT('Ctrl Pts',(19.2311796388619,-1.3390663121984,339.734439181957));
#67121=CARTESIAN_POINT('Ctrl Pts',(19.2234307538338,-1.20643434800378,339.769957998922));
#67122=CARTESIAN_POINT('Ctrl Pts',(19.2156818688057,-1.07262145102994,339.799861069374));
#67123=CARTESIAN_POINT('Ctrl Pts',(19.207924759031,-0.938666523664893,339.829795879254));
#67124=CARTESIAN_POINT('Ctrl Pts',(19.2001676492563,-0.803528541696102,
339.854102950361));
#67125=CARTESIAN_POINT('Ctrl Pts',(19.1924105394816,-0.667719243133995,
339.872713214919));
#67126=CARTESIAN_POINT('Ctrl Pts',(19.1846492845554,-0.531837372424799,
339.891333424208));
#67127=CARTESIAN_POINT('Ctrl Pts',(19.1768880296292,-0.395283859259923,
339.904250724331));
#67128=CARTESIAN_POINT('Ctrl Pts',(19.169126774703,-0.258573832245395,339.911448120033));
#67129=CARTESIAN_POINT('Ctrl Pts',(19.1613531042984,-0.121645113741525,
339.918657029223));
#67130=CARTESIAN_POINT('Ctrl Pts',(19.1535794338937,0.0154402278703251,
339.920127745421));
#67131=CARTESIAN_POINT('Ctrl Pts',(19.145805763489,0.152167902481845,339.91589544152));
#67132=CARTESIAN_POINT('Ctrl Pts',(19.138393959312,0.282530870945051,339.911860152383));
#67133=CARTESIAN_POINT('Ctrl Pts',(19.1309821551349,0.412568434761274,339.902640865946));
#67134=CARTESIAN_POINT('Ctrl Pts',(19.1235703509578,0.54184249212369,339.88831154656));
#67135=CARTESIAN_POINT('Ctrl Pts',(19.1157952721794,0.677452656125461,339.873279904546));
#67136=CARTESIAN_POINT('Ctrl Pts',(19.1080201934009,0.812651130976679,339.852577145278));
#67137=CARTESIAN_POINT('Ctrl Pts',(19.1002451146225,0.946925770113189,339.826231930647));
#67138=CARTESIAN_POINT('Ctrl Pts',(19.0924796035735,1.08103517575808,339.79991913548));
#67139=CARTESIAN_POINT('Ctrl Pts',(19.0847140925244,1.21422262777671,339.767977774863));
#67140=CARTESIAN_POINT('Ctrl Pts',(19.0769485814754,1.34598046936304,339.730488308684));
#67141=CARTESIAN_POINT('Ctrl Pts',(19.0691907699532,1.47760767266575,339.693036013419));
#67142=CARTESIAN_POINT('Ctrl Pts',(19.061432958431,1.60780771283721,339.650046666101));
#67143=CARTESIAN_POINT('Ctrl Pts',(19.0536751469088,1.73608286082123,339.601651808086));
#67144=CARTESIAN_POINT('Ctrl Pts',(19.0459231733858,1.86426147768855,339.553293368737));
#67145=CARTESIAN_POINT('Ctrl Pts',(19.0381711998628,1.99051772138093,339.499537652904));
#67146=CARTESIAN_POINT('Ctrl Pts',(19.0304192263397,2.11436912077686,339.440565986854));
#67147=CARTESIAN_POINT('Ctrl Pts',(19.0226705357821,2.23816806903145,339.38161929534));
#67148=CARTESIAN_POINT('Ctrl Pts',(19.0149218452245,2.3595638464446,339.31746121476));
#67149=CARTESIAN_POINT('Ctrl Pts',(19.0071731546669,2.47809427619279,339.248321059054));
#67150=CARTESIAN_POINT('Ctrl Pts',(18.999426076289,2.59660004469509,339.179195288534));
#67151=CARTESIAN_POINT('Ctrl Pts',(18.9916789979112,2.71224131391566,339.105089701505));
#67152=CARTESIAN_POINT('Ctrl Pts',(18.9839319195334,2.8245811788693,339.026279203741));
#67153=CARTESIAN_POINT('Ctrl Pts',(18.9761847762276,2.93692198533937,338.947468045469));
#67154=CARTESIAN_POINT('Ctrl Pts',(18.9684376329218,3.04596101236914,338.863952122293));
#67155=CARTESIAN_POINT('Ctrl Pts',(18.960690489616,3.15129131384103,338.776049008926));
#67156=CARTESIAN_POINT('Ctrl Pts',(18.9529416045879,3.25664529580049,338.688126133073));
#67157=CARTESIAN_POINT('Ctrl Pts',(18.9451927195598,3.35828859299271,338.595814354732));
#67158=CARTESIAN_POINT('Ctrl Pts',(18.9374438345317,3.4558485596247,338.499470502153));
#67159=CARTESIAN_POINT('Ctrl Pts',(18.929686724757,3.55351207741353,338.403024389214));
#67160=CARTESIAN_POINT('Ctrl Pts',(18.9219296149823,3.64708332833514,338.302537928049));
#67161=CARTESIAN_POINT('Ctrl Pts',(18.9141725052075,3.73622730102274,338.198404073533));
#67162=CARTESIAN_POINT('Ctrl Pts',(18.9064112502813,3.82541890939914,338.094214573214));
#67163=CARTESIAN_POINT('Ctrl Pts',(18.8986499953552,3.91017828406342,337.986374103044));
#67164=CARTESIAN_POINT('Ctrl Pts',(18.890888740429,3.99021236769644,337.875306648548));
#67165=CARTESIAN_POINT('Ctrl Pts',(18.8831150700244,4.07037447978013,337.764061522321));
#67166=CARTESIAN_POINT('Ctrl Pts',(18.8753413996197,4.14579598070891,337.649579422897));
#67167=CARTESIAN_POINT('Ctrl Pts',(18.867567729215,4.21622813623038,337.532311861868));
#67168=CARTESIAN_POINT('Ctrl Pts',(18.860155925038,4.28338165796657,337.42050313402));
#67169=CARTESIAN_POINT('Ctrl Pts',(18.852744120861,4.34599975065074,337.306162687484));
#67170=CARTESIAN_POINT('Ctrl Pts',(18.845332316684,4.40390753045873,337.189698957772));
#67171=CARTESIAN_POINT('Ctrl Pts',(18.8375572379056,4.46465354305414,337.067526993738));
#67172=CARTESIAN_POINT('Ctrl Pts',(18.8297821591271,4.52040780354033,336.942632260939));
#67173=CARTESIAN_POINT('Ctrl Pts',(18.8220070803487,4.57091726242068,336.815460944941));
#67174=CARTESIAN_POINT('Ctrl Pts',(18.8142415692997,4.62136456619628,336.688446121343));
#67175=CARTESIAN_POINT('Ctrl Pts',(18.8064760582507,4.66657976719625,336.559160648486));
#67176=CARTESIAN_POINT('Ctrl Pts',(18.7987105472017,4.70635580362896,336.428074967272));
#67177=CARTESIAN_POINT('Ctrl Pts',(18.7909527356795,4.74609240200571,336.297119257892));
#67178=CARTESIAN_POINT('Ctrl Pts',(18.7831949241573,4.78040045532157,336.164367263854));
#67179=CARTESIAN_POINT('Ctrl Pts',(18.7754371126351,4.8091212297588,336.030308720716));
#67180=CARTESIAN_POINT('Ctrl Pts',(18.7676851391121,4.8378203909024,335.896351060884));
#67181=CARTESIAN_POINT('Ctrl Pts',(18.7599331655891,4.86094056067386,335.761089189665));
#67182=CARTESIAN_POINT('Ctrl Pts',(18.7521811920662,4.87837312739248,335.625026953367));
#67183=CARTESIAN_POINT('Ctrl Pts',(18.7444325015085,4.89579831140878,335.489022339506));
#67184=CARTESIAN_POINT('Ctrl Pts',(18.736683810951,4.90754063354313,335.352218421623));
#67185=CARTESIAN_POINT('Ctrl Pts',(18.7289351203933,4.91354281838064,335.215127948998));
#67186=CARTESIAN_POINT('Ctrl Pts',(18.7211880420155,4.91954375441347,335.078065999191));
#67187=CARTESIAN_POINT('Ctrl Pts',(18.7134409636377,4.91980691157742,334.940718003486));
#67188=CARTESIAN_POINT('Ctrl Pts',(18.7056938852598,4.91432702964588,334.803600131894));
#67189=CARTESIAN_POINT('Ctrl Pts',(18.6979467419541,4.90884710178767,334.666481111124));
#67190=CARTESIAN_POINT('Ctrl Pts',(18.6901995986482,4.89762405443946,334.529592608876));
#67191=CARTESIAN_POINT('Ctrl Pts',(18.6824524553425,4.88070472105624,334.393448692723));
#67192=CARTESIAN_POINT('Ctrl Pts',(18.6747035703144,4.86378158384762,334.257274168527));
#67193=CARTESIAN_POINT('Ctrl Pts',(18.6669546852863,4.84115966045721,334.121844951344));
#67194=CARTESIAN_POINT('Ctrl Pts',(18.6592058002582,4.81293735535237,333.987667507212));
#67195=CARTESIAN_POINT('Ctrl Pts',(18.6514486904835,4.78468509480134,333.853347645756));
#67196=CARTESIAN_POINT('Ctrl Pts',(18.6436915807087,4.75082065881443,333.720282594553));
#67197=CARTESIAN_POINT('Ctrl Pts',(18.635934470934,4.71149319765503,333.588966722238));
#67198=CARTESIAN_POINT('Ctrl Pts',(18.6281732160078,4.67214472115781,333.457580678921));
#67199=CARTESIAN_POINT('Ctrl Pts',(18.6204119610816,4.62732753023863,333.327946046209));
#67200=CARTESIAN_POINT('Ctrl Pts',(18.6126507061555,4.57723957324151,333.200538705153));
#67201=CARTESIAN_POINT('Ctrl Pts',(18.6048770357508,4.52707149183689,333.072927553873));
#67202=CARTESIAN_POINT('Ctrl Pts',(18.5971033653462,4.47161595390004,332.947551171715));
#67203=CARTESIAN_POINT('Ctrl Pts',(18.5893296949415,4.41111804078659,332.824863063449));
#67204=CARTESIAN_POINT('Ctrl Pts',(18.5819178907644,4.35343632008304,332.707886116139));
#67205=CARTESIAN_POINT('Ctrl Pts',(18.5745060865872,4.29117124222047,332.593353049627));
#67206=CARTESIAN_POINT('Ctrl Pts',(18.5670942824101,4.22457162966154,332.481631955341));
#67207=CARTESIAN_POINT('Ctrl Pts',(18.5593192036316,4.15470777170164,332.364435077426));
#67208=CARTESIAN_POINT('Ctrl Pts',(18.5515441248532,4.07985295590634,332.249962423942));
#67209=CARTESIAN_POINT('Ctrl Pts',(18.5437690460748,4.00024544963459,332.138668246222));
#67210=CARTESIAN_POINT('Ctrl Pts',(18.5360035350258,3.92073590546758,332.027511023074));
#67211=CARTESIAN_POINT('Ctrl Pts',(18.5282380239768,3.83648553286708,331.919524808168));
#67212=CARTESIAN_POINT('Ctrl Pts',(18.5204725129279,3.7477778826058,331.815138306747));
#67213=CARTESIAN_POINT('Ctrl Pts',(18.5127147014057,3.65915818623771,331.710855304846));
#67214=CARTESIAN_POINT('Ctrl Pts',(18.5049568898834,3.56609025855625,331.6101652096));
#67215=CARTESIAN_POINT('Ctrl Pts',(18.4971990783612,3.46890002866377,331.513466527676));
#67216=CARTESIAN_POINT('Ctrl Pts',(18.4894471048383,3.37178293750176,331.416840614576));
#67217=CARTESIAN_POINT('Ctrl Pts',(18.4816951313153,3.2705499948068,331.324200410727));
#67218=CARTESIAN_POINT('Ctrl Pts',(18.4739431577923,3.1655661196753,331.235909910156));
#67219=CARTESIAN_POINT('Ctrl Pts',(18.4661944672347,3.06062670527681,331.147656800663));
#67220=CARTESIAN_POINT('Ctrl Pts',(18.4584457766771,2.951939816426,331.063749981695));
#67221=CARTESIAN_POINT('Ctrl Pts',(18.4506970861195,2.83990563991946,330.984515095427));
#67222=CARTESIAN_POINT('Ctrl Pts',(18.4429500077416,2.72789477305907,330.905296694639));
#67223=CARTESIAN_POINT('Ctrl Pts',(18.4352029293638,2.61253832272112,330.830748518663));
#67224=CARTESIAN_POINT('Ctrl Pts',(18.427455850986,2.49426750066995,330.761154320148));
#67225=CARTESIAN_POINT('Ctrl Pts',(18.4197087076802,2.37599568739553,330.691559538366));
#67226=CARTESIAN_POINT('Ctrl Pts',(18.4119615643744,2.25480979056905,330.626919015088));
#67227=CARTESIAN_POINT('Ctrl Pts',(18.4042144210686,2.13116744484765,330.567471558521));
#67228=CARTESIAN_POINT('Ctrl Pts',(18.3964655360405,2.00749730170211,330.508010736904));
#67229=CARTESIAN_POINT('Ctrl Pts',(18.3887166510124,1.88136996292533,330.453745474556));
#67230=CARTESIAN_POINT('Ctrl Pts',(18.3809677659843,1.75326457891779,330.404867098896));
#67231=CARTESIAN_POINT('Ctrl Pts',(18.3732106562096,1.62502322253156,330.355936843222));
#67232=CARTESIAN_POINT('Ctrl Pts',(18.3654535464348,1.49479999270271,330.312405035432));
#67233=CARTESIAN_POINT('Ctrl Pts',(18.35769643666,1.36309132832952,330.274413783124));
#67234=CARTESIAN_POINT('Ctrl Pts',(18.3499351817339,1.23131228305759,330.236402229504));
#67235=CARTESIAN_POINT('Ctrl Pts',(18.3421739268077,1.09804660116079,330.203937223287));
#67236=CARTESIAN_POINT('Ctrl Pts',(18.3344126718816,0.96380158237269,330.177109832029));
#67237=CARTESIAN_POINT('Ctrl Pts',(18.3266390014769,0.829341815304878,330.150239525687));
#67238=CARTESIAN_POINT('Ctrl Pts',(18.3188653310722,0.693899967144402,330.129024916149));
#67239=CARTESIAN_POINT('Ctrl Pts',(18.3110916606676,0.557990027312234,330.113505326728));
#67240=CARTESIAN_POINT('Ctrl Pts',(18.3036798564904,0.428406727876556,330.098708177927));
#67241=CARTESIAN_POINT('Ctrl Pts',(18.2962680523133,0.298398222389613,330.089087796073));
#67242=CARTESIAN_POINT('Ctrl Pts',(18.2888562481362,0.168408698899535,330.084634136442));
#67243=CARTESIAN_POINT('Ctrl Pts',(18.2810811693578,0.0320480016448979,
330.079962189685));
#67244=CARTESIAN_POINT('Ctrl Pts',(18.2733060905793,-0.104722730832196,
330.080961480005));
#67245=CARTESIAN_POINT('Ctrl Pts',(18.2655310118008,-0.241392568755692,
330.087677464758));
#67246=CARTESIAN_POINT('Ctrl Pts',(18.2577655007518,-0.377894225742424,
330.094385185064));
#67247=CARTESIAN_POINT('Ctrl Pts',(18.2499999897029,-0.514294848541628,
330.106795583653));
#67248=CARTESIAN_POINT('Ctrl Pts',(18.2422344786538,-0.65008048417517,330.124902213638));
#67249=CARTESIAN_POINT('Ctrl Pts',(18.2344766671316,-0.785731487955745,
330.142990890846));
#67250=CARTESIAN_POINT('Ctrl Pts',(18.2267188556095,-0.920768333081667,
330.166764508617));
#67251=CARTESIAN_POINT('Ctrl Pts',(18.2189610440873,-1.05467952785701,330.196164641037));
#67252=CARTESIAN_POINT('Ctrl Pts',(18.2112090705643,-1.18848995021189,330.225542648926));
#67253=CARTESIAN_POINT('Ctrl Pts',(18.2034570970412,-1.32117602805858,330.260538660152));
#67254=CARTESIAN_POINT('Ctrl Pts',(18.1957051235182,-1.45223419239217,330.301042784516));
#67255=CARTESIAN_POINT('Ctrl Pts',(18.1879564329605,-1.58323685351517,330.341529755359));
#67256=CARTESIAN_POINT('Ctrl Pts',(18.180207742403,-1.71261259966859,330.387520084611));
#67257=CARTESIAN_POINT('Ctrl Pts',(18.1724590518454,-1.83987102736082,330.438853470324));
#67258=CARTESIAN_POINT('Ctrl Pts',(18.1647119734675,-1.96710297787445,330.490176175696));
#67259=CARTESIAN_POINT('Ctrl Pts',(18.1569648950896,-2.09221812389769,330.546839580214));
#67260=CARTESIAN_POINT('Ctrl Pts',(18.1492178167118,-2.21474449834672,330.608634623543));
#67261=CARTESIAN_POINT('Ctrl Pts',(18.1414706734059,-2.33727189968494,330.670430184775));
#67262=CARTESIAN_POINT('Ctrl Pts',(18.1337235301001,-2.45721013717334,330.737357294586));
#67263=CARTESIAN_POINT('Ctrl Pts',(18.1259763867943,-2.57411073952276,330.809160351055));
#67264=CARTESIAN_POINT('Ctrl Pts',(18.1182275017662,-2.69103762360882,330.880979550374));
#67265=CARTESIAN_POINT('Ctrl Pts',(18.1104786167381,-2.80492518061293,330.957676673164));
#67266=CARTESIAN_POINT('Ctrl Pts',(18.10272973171,-2.91535322345182,331.038952329874));
#67267=CARTESIAN_POINT('Ctrl Pts',(18.0949726219353,-3.02589847575661,331.120314253406));
#67268=CARTESIAN_POINT('Ctrl Pts',(18.0872155121606,-3.13297656350486,331.206264186511));
#67269=CARTESIAN_POINT('Ctrl Pts',(18.0794584023859,-3.2361993338129,331.296461565701));
#67270=CARTESIAN_POINT('Ctrl Pts',(18.0716971474597,-3.33947726306918,331.386707143487));
#67271=CARTESIAN_POINT('Ctrl Pts',(18.0639358925335,-3.4388954866653,331.481204420788));
#67272=CARTESIAN_POINT('Ctrl Pts',(18.0561746376073,-3.53410289495589,331.579576080313));
#67273=CARTESIAN_POINT('Ctrl Pts',(18.0484009672026,-3.62946260407147,331.678105102435));
#67274=CARTESIAN_POINT('Ctrl Pts',(18.0406272967979,-3.7205977775169,331.780520599563));
#67275=CARTESIAN_POINT('Ctrl Pts',(18.0328536263933,-3.807197198311,331.88641162713));
#67276=CARTESIAN_POINT('Ctrl Pts',(18.0254418222163,-3.88976539523146,331.987373401886));
#67277=CARTESIAN_POINT('Ctrl Pts',(18.0180300180393,-3.96821044177837,332.091494187119));
#67278=CARTESIAN_POINT('Ctrl Pts',(18.0106182138623,-4.04230040913374,332.198395019847));
#67279=CARTESIAN_POINT('Ctrl Pts',(18.0027430572091,-4.12102214616636,332.311978809164));
#67280=CARTESIAN_POINT('Ctrl Pts',(17.9948679005558,-4.19507219954527,332.429055015561));
#67281=CARTESIAN_POINT('Ctrl Pts',(17.9869927439025,-4.26412989625754,332.549208435966));
#67282=CARTESIAN_POINT('Ctrl Pts',(17.9791278749331,-4.33309737968518,332.669204894363));
#67283=CARTESIAN_POINT('Ctrl Pts',(17.9712630059637,-4.39708529984977,332.792270242156));
#67284=CARTESIAN_POINT('Ctrl Pts',(17.9633981369942,-4.45581496266319,332.91795867452));
#67285=CARTESIAN_POINT('Ctrl Pts',(17.9555419936708,-4.51447946809779,333.043507662378));
#67286=CARTESIAN_POINT('Ctrl Pts',(17.9476858503473,-4.56789716993842,333.171673602145));
#67287=CARTESIAN_POINT('Ctrl Pts',(17.9398297070238,-4.61583432718745,333.301984532916));
#67288=CARTESIAN_POINT('Ctrl Pts',(17.9316620128142,-4.66567252712435,333.437463201122));
#67289=CARTESIAN_POINT('Ctrl Pts',(17.9234943186047,-4.70958633391736,333.575260143042));
#67290=CARTESIAN_POINT('Ctrl Pts',(17.9153266243951,-4.74736692646326,333.714818951267));
#67291=CARTESIAN_POINT('Ctrl Pts',(17.9074841982159,-4.78364295497812,333.848820007511));
#67292=CARTESIAN_POINT('Ctrl Pts',(17.8996417720367,-4.81426473902137,333.984444899537));
#67293=CARTESIAN_POINT('Ctrl Pts',(17.8917993458575,-4.83909747893079,334.121183379819));
#67294=CARTESIAN_POINT('Ctrl Pts',(17.8839605331121,-4.86391877704156,334.257858857221));
#67295=CARTESIAN_POINT('Ctrl Pts',(17.8761217203666,-4.88295627539233,334.395646530158));
#67296=CARTESIAN_POINT('Ctrl Pts',(17.8682829076212,-4.89612605567246,334.534024990514));
#67297=CARTESIAN_POINT('Ctrl Pts',(17.8604460906169,-4.90929248296112,334.672368220078));
#67298=CARTESIAN_POINT('Ctrl Pts',(17.8526092736126,-4.91659413243677,334.811301561753));
#67299=CARTESIAN_POINT('Ctrl Pts',(17.8447724566083,-4.91799885567452,334.950297705445));
#67300=CARTESIAN_POINT('Ctrl Pts',(17.8437874299084,-4.91817541841605,334.967768435288));
#67301=CARTESIAN_POINT('Ctrl Pts',(17.8428024032086,-4.91825888585813,334.985240153472));
#67302=CARTESIAN_POINT('Ctrl Pts',(17.8418173765088,-4.91824925238482,335.002711810498));
#67303=CARTESIAN_POINT('',(16.0918173765465,-4.91824914986108,335.002891779856));
#67304=CARTESIAN_POINT('Ctrl Pts',(17.841817376457,-4.91824925238431,335.002711811417));
#67305=CARTESIAN_POINT('Ctrl Pts',(17.8332302331793,-4.91816527086008,335.155024050462));
#67306=CARTESIAN_POINT('Ctrl Pts',(17.8246430899017,-4.91100184266203,335.307084674523));
#67307=CARTESIAN_POINT('Ctrl Pts',(17.8160559466241,-4.89685328824803,335.458269501357));
#67308=CARTESIAN_POINT('Ctrl Pts',(17.8074201728907,-4.88262460815933,335.610310513629));
#67309=CARTESIAN_POINT('Ctrl Pts',(17.7987843991574,-4.86133154917201,335.76146555601));
#67310=CARTESIAN_POINT('Ctrl Pts',(17.7901486254241,-4.83312016722997,335.911116080209));
#67311=CARTESIAN_POINT('Ctrl Pts',(17.7814876028616,-4.80482630230683,336.061204144879));
#67312=CARTESIAN_POINT('Ctrl Pts',(17.7728265802992,-4.76957371770995,336.209778671613));
#67313=CARTESIAN_POINT('Ctrl Pts',(17.7641655577368,-4.72755845325742,336.356235279564));
#67314=CARTESIAN_POINT('Ctrl Pts',(17.7554727122363,-4.68538881336621,336.503230008681));
#67315=CARTESIAN_POINT('Ctrl Pts',(17.7467798667357,-4.63640682438824,336.648091022477));
#67316=CARTESIAN_POINT('Ctrl Pts',(17.7380870212353,-4.58085791823456,336.790230095671));
#67317=CARTESIAN_POINT('Ctrl Pts',(17.7361847406862,-4.56870199027179,336.82133480059));
#67318=CARTESIAN_POINT('Ctrl Pts',(17.7342824601373,-4.55623176176412,336.852309250801));
#67319=CARTESIAN_POINT('Ctrl Pts',(17.7323801795882,-4.54345009596233,336.883147441917));
#67320=CARTESIAN_POINT('Ctrl Pts',(17.7246051008098,-4.49120834929648,337.009190556556));
#67321=CARTESIAN_POINT('Ctrl Pts',(17.7168300220313,-4.43363509748446,337.133257282632));
#67322=CARTESIAN_POINT('Ctrl Pts',(17.7090549432528,-4.37090064476501,337.254863768855));
#67323=CARTESIAN_POINT('Ctrl Pts',(17.7012894322037,-4.30824339078349,337.376320610554));
#67324=CARTESIAN_POINT('Ctrl Pts',(17.6935239211546,-4.24043775042469,337.495322892166));
#67325=CARTESIAN_POINT('Ctrl Pts',(17.6857584101056,-4.16770252064172,337.611405514648));
#67326=CARTESIAN_POINT('Ctrl Pts',(17.6780005985834,-4.0950394080509,337.727373040873));
#67327=CARTESIAN_POINT('Ctrl Pts',(17.6702427870611,-4.01745663904239,337.840426339792));
#67328=CARTESIAN_POINT('Ctrl Pts',(17.6624849755389,-3.93521929913768,337.950124087254));
#67329=CARTESIAN_POINT('Ctrl Pts',(17.6547330020159,-3.85304384543915,338.059739283681));
#67330=CARTESIAN_POINT('Ctrl Pts',(17.6469810284928,-3.7662210263367,338.166003643366));
#67331=CARTESIAN_POINT('Ctrl Pts',(17.6392290549698,-3.67505948478858,338.268504374445));
#67332=CARTESIAN_POINT('Ctrl Pts',(17.6314803644122,-3.58393655020742,338.370961696403));
#67333=CARTESIAN_POINT('Ctrl Pts',(17.6237316738546,-3.48847880696359,338.469658268443));
#67334=CARTESIAN_POINT('Ctrl Pts',(17.6159829832969,-3.3890353254058,338.564214166636));
#67335=CARTESIAN_POINT('Ctrl Pts',(17.608235904919,-3.28961253389491,338.658750391686));
#67336=CARTESIAN_POINT('Ctrl Pts',(17.6004888265411,-3.18620593662452,338.749147387305));
#67337=CARTESIAN_POINT('Ctrl Pts',(17.5927417481633,-3.07920134282074,338.835062209778));
#67338=CARTESIAN_POINT('Ctrl Pts',(17.5849946048574,-2.97219585221554,338.920977752301));
#67339=CARTESIAN_POINT('Ctrl Pts',(17.5772474615517,-2.86159260971993,339.002410802035));
#67340=CARTESIAN_POINT('Ctrl Pts',(17.5695003182458,-2.74781004974923,339.079059081822));
#67341=CARTESIAN_POINT('Ctrl Pts',(17.5617514332177,-2.63400190904338,339.155724593771));
#67342=CARTESIAN_POINT('Ctrl Pts',(17.5540025481896,-2.5170133526508,339.227602976877));
#67343=CARTESIAN_POINT('Ctrl Pts',(17.5462536631615,-2.39729094985445,339.294435837714));
#67344=CARTESIAN_POINT('Ctrl Pts',(17.5384965533867,-2.27744147246264,339.361339635641));
#67345=CARTESIAN_POINT('Ctrl Pts',(17.530739443612,-2.15485269401971,339.423187022623));
#67346=CARTESIAN_POINT('Ctrl Pts',(17.5229823338372,-2.02999538623468,339.479765819143));
#67347=CARTESIAN_POINT('Ctrl Pts',(17.515221078911,-1.90507135869679,339.536374849564));
#67348=CARTESIAN_POINT('Ctrl Pts',(17.5074598239849,-1.77787674862338,339.587709533438));
#67349=CARTESIAN_POINT('Ctrl Pts',(17.4996985690587,-1.64890043197093,339.633606632845));
#67350=CARTESIAN_POINT('Ctrl Pts',(17.491924898654,-1.51971779524494,339.679577152654));
#67351=CARTESIAN_POINT('Ctrl Pts',(17.4841512282493,-1.38874813010787,339.720092590514));
#67352=CARTESIAN_POINT('Ctrl Pts',(17.4763775578446,-1.25649439067527,339.755039948171));
#67353=CARTESIAN_POINT('Ctrl Pts',(17.4689657536678,-1.13039709463704,339.78836049792));
#67354=CARTESIAN_POINT('Ctrl Pts',(17.461553949491,-1.00313286223564,339.816619627343));
#67355=CARTESIAN_POINT('Ctrl Pts',(17.4541421453142,-0.875142690937076,
339.839763251751));
#67356=CARTESIAN_POINT('Ctrl Pts',(17.4463670665358,-0.740879340074871,
339.864041214134));
#67357=CARTESIAN_POINT('Ctrl Pts',(17.4385919877574,-0.605392793162187,
339.882766262841));
#67358=CARTESIAN_POINT('Ctrl Pts',(17.430816908979,-0.469182092469226,339.895819770642));
#67359=CARTESIAN_POINT('Ctrl Pts',(17.42305139793,-0.333139007715249,339.90885721527));
#67360=CARTESIAN_POINT('Ctrl Pts',(17.415285886881,-0.196373927621072,339.916236968652));
#67361=CARTESIAN_POINT('Ctrl Pts',(17.407520375832,-0.0593963674799437,
339.917891330035));
#67362=CARTESIAN_POINT('Ctrl Pts',(17.3997625643097,0.0774453790117849,
339.919544051113));
#67363=CARTESIAN_POINT('Ctrl Pts',(17.3920047527875,0.214498797968074,339.91548267254));
#67364=CARTESIAN_POINT('Ctrl Pts',(17.3842469412653,0.351249317506626,339.905691284564));
#67365=CARTESIAN_POINT('Ctrl Pts',(17.3764949677423,0.487896927942431,339.895907264919));
#67366=CARTESIAN_POINT('Ctrl Pts',(17.3687429942193,0.624241704360384,339.880401846525));
#67367=CARTESIAN_POINT('Ctrl Pts',(17.3609910206963,0.759769496860928,339.859211188469));
#67368=CARTESIAN_POINT('Ctrl Pts',(17.3532423301387,0.895239893260885,339.838029504669));
#67369=CARTESIAN_POINT('Ctrl Pts',(17.345493639581,1.02989360852097,339.811167430212));
#67370=CARTESIAN_POINT('Ctrl Pts',(17.3377449490234,1.16322225450981,339.778712907166));
#67371=CARTESIAN_POINT('Ctrl Pts',(17.3299978706456,1.29652316036027,339.746265136554));
#67372=CARTESIAN_POINT('Ctrl Pts',(17.3222507922677,1.4284991657636,339.708227324135));
#67373=CARTESIAN_POINT('Ctrl Pts',(17.3145037138899,1.55865309852318,339.664738318595));
#67374=CARTESIAN_POINT('Ctrl Pts',(17.3067565705841,1.68880812209789,339.621248948575));
#67375=CARTESIAN_POINT('Ctrl Pts',(17.2990094272783,1.8171406718436,339.572308418182));
#67376=CARTESIAN_POINT('Ctrl Pts',(17.2912622839725,1.94317011757803,339.518105018329));
#67377=CARTESIAN_POINT('Ctrl Pts',(17.2835133989445,2.06922789740754,339.463889432401));
#67378=CARTESIAN_POINT('Ctrl Pts',(17.2757645139163,2.19298118388524,339.404408776969));
#67379=CARTESIAN_POINT('Ctrl Pts',(17.2680156288882,2.31397102420308,339.339898750161));
#67380=CARTESIAN_POINT('Ctrl Pts',(17.2602585191135,2.43508928438749,339.275320251744));
#67381=CARTESIAN_POINT('Ctrl Pts',(17.2525014093388,2.55343789371412,339.205701902533));
#67382=CARTESIAN_POINT('Ctrl Pts',(17.244744299564,2.66858366431691,339.131324761991));
#67383=CARTESIAN_POINT('Ctrl Pts',(17.2369830446379,2.78379096513778,339.056907876684));
#67384=CARTESIAN_POINT('Ctrl Pts',(17.2292217897117,2.8957916979206,338.977727358523));
#67385=CARTESIAN_POINT('Ctrl Pts',(17.2214605347856,3.0041840335839,338.894105976326));
#67386=CARTESIAN_POINT('Ctrl Pts',(17.2136868643809,3.11274976165943,338.81035082717));
#67387=CARTESIAN_POINT('Ctrl Pts',(17.2059131939763,3.21769525855827,338.722140869843));
#67388=CARTESIAN_POINT('Ctrl Pts',(17.1981395235716,3.31865332430625,338.629837899352));
#67389=CARTESIAN_POINT('Ctrl Pts',(17.1907277193945,3.41491176780441,338.541831654344));
#67390=CARTESIAN_POINT('Ctrl Pts',(17.1833159152174,3.50754545119424,338.450105082691));
#67391=CARTESIAN_POINT('Ctrl Pts',(17.1759041110404,3.59627024447424,338.35499976024));
#67392=CARTESIAN_POINT('Ctrl Pts',(17.1681290322619,3.68934370417048,338.255233042632));
#67393=CARTESIAN_POINT('Ctrl Pts',(17.1603539534835,3.7784095418604,338.151432713152));
#67394=CARTESIAN_POINT('Ctrl Pts',(17.1525788747051,3.86309794096781,338.043954231093));
#67395=CARTESIAN_POINT('Ctrl Pts',(17.1448133636561,3.94768212560859,337.936608008149));
#67396=CARTESIAN_POINT('Ctrl Pts',(17.137047852607,4.02789935008547,337.825592942548));
#67397=CARTESIAN_POINT('Ctrl Pts',(17.129282341558,4.10341695542925,337.711300859808));
#67398=CARTESIAN_POINT('Ctrl Pts',(17.1215245300358,4.17885968484752,337.597122098001));
#67399=CARTESIAN_POINT('Ctrl Pts',(17.1137667185136,4.24961185408082,337.479673109107));
#67400=CARTESIAN_POINT('Ctrl Pts',(17.1060089069914,4.31538161990733,337.359377997919));
#67401=CARTESIAN_POINT('Ctrl Pts',(17.0982569334684,4.38110189189929,337.239173412618));
#67402=CARTESIAN_POINT('Ctrl Pts',(17.0905049599455,4.44184703676003,337.116127309747));
#67403=CARTESIAN_POINT('Ctrl Pts',(17.0827529864225,4.49736922542266,336.99069161668));
#67404=CARTESIAN_POINT('Ctrl Pts',(17.0750042958649,4.55286790040543,336.865309045705));
#67405=CARTESIAN_POINT('Ctrl Pts',(17.0672556053073,4.60314786067368,336.737539253998));
#67406=CARTESIAN_POINT('Ctrl Pts',(17.0595069147496,4.64800794059774,336.607857346483));
#67407=CARTESIAN_POINT('Ctrl Pts',(17.0517598363718,4.69285868700756,336.478202420373));
#67408=CARTESIAN_POINT('Ctrl Pts',(17.044012757994,4.73229166834846,336.346636538935));
#67409=CARTESIAN_POINT('Ctrl Pts',(17.0362656796161,4.76615459703989,336.213652923869));
#67410=CARTESIAN_POINT('Ctrl Pts',(17.0285185363103,4.80001780953523,336.080668194272));
#67411=CARTESIAN_POINT('Ctrl Pts',(17.0207713930045,4.82831077981538,335.946266086133));
#67412=CARTESIAN_POINT('Ctrl Pts',(17.0130242496987,4.85093174915527,335.810952666644));
#67413=CARTESIAN_POINT('Ctrl Pts',(17.0052753646706,4.8735578041693,335.675608825826));
#67414=CARTESIAN_POINT('Ctrl Pts',(16.9975264796425,4.89050925632769,335.539353651413));
#67415=CARTESIAN_POINT('Ctrl Pts',(16.9897775946145,4.90173594351511,335.402700636394));
#67416=CARTESIAN_POINT('Ctrl Pts',(16.9820204848397,4.91297454682432,335.265902576453));
#67417=CARTESIAN_POINT('Ctrl Pts',(16.974263375065,4.91847621507906,335.128706222555));
#67418=CARTESIAN_POINT('Ctrl Pts',(16.9665062652903,4.91824287436707,334.991627949022));
#67419=CARTESIAN_POINT('Ctrl Pts',(16.9587450103641,4.91800940896526,334.854476425241));
#67420=CARTESIAN_POINT('Ctrl Pts',(16.950983755438,4.91203484511147,334.717443497859));
#67421=CARTESIAN_POINT('Ctrl Pts',(16.9432225005118,4.90037315321631,334.58104174225));
#67422=CARTESIAN_POINT('Ctrl Pts',(16.9354488301072,4.88869280641467,334.444421788285));
#67423=CARTESIAN_POINT('Ctrl Pts',(16.9276751597025,4.87130720156489,334.308435411633));
#67424=CARTESIAN_POINT('Ctrl Pts',(16.9199014892979,4.84832186683064,334.173587186624));
#67425=CARTESIAN_POINT('Ctrl Pts',(16.9124896851208,4.82640650495809,334.045016178931));
#67426=CARTESIAN_POINT('Ctrl Pts',(16.9050778809436,4.7994010753556,333.917480027123));
#67427=CARTESIAN_POINT('Ctrl Pts',(16.8976660767665,4.76743905739485,333.791402508473));
#67428=CARTESIAN_POINT('Ctrl Pts',(16.8898909979881,4.73391048572407,333.659145555068));
#67429=CARTESIAN_POINT('Ctrl Pts',(16.8821159192096,4.69482120955295,333.528075877675));
#67430=CARTESIAN_POINT('Ctrl Pts',(16.8743408404312,4.65027001321283,333.398696822362));
#67431=CARTESIAN_POINT('Ctrl Pts',(16.8665753293822,4.60577363995606,333.269476976213));
#67432=CARTESIAN_POINT('Ctrl Pts',(16.8588098183332,4.55582884591748,333.141943978751));
#67433=CARTESIAN_POINT('Ctrl Pts',(16.8510443072842,4.50058510467792,333.016589609271));
#67434=CARTESIAN_POINT('Ctrl Pts',(16.843286495762,4.4453961377686,332.891359529014));
#67435=CARTESIAN_POINT('Ctrl Pts',(16.8355286842398,4.38491883587396,332.768304133362));
#67436=CARTESIAN_POINT('Ctrl Pts',(16.8277708727176,4.31935190464974,332.647898346946));
#67437=CARTESIAN_POINT('Ctrl Pts',(16.8200188991946,4.2538343146206,332.527583169703));
#67438=CARTESIAN_POINT('Ctrl Pts',(16.8122669256716,4.18323490508244,332.409913974801));
#67439=CARTESIAN_POINT('Ctrl Pts',(16.8045149521486,4.10779959687776,332.295343730824));
#67440=CARTESIAN_POINT('Ctrl Pts',(16.796766261591,4.03239623557089,332.180822007414));
#67441=CARTESIAN_POINT('Ctrl Pts',(16.7890175710333,3.95216126344027,332.069396950426));
#67442=CARTESIAN_POINT('Ctrl Pts',(16.7812688804757,3.86738534408705,331.961494830868));
#67443=CARTESIAN_POINT('Ctrl Pts',(16.7735218020979,3.78262706307192,331.853615161247));
#67444=CARTESIAN_POINT('Ctrl Pts',(16.7657747237201,3.69332995540377,331.749257278277));
#67445=CARTESIAN_POINT('Ctrl Pts',(16.7580276453423,3.59982637018302,331.648816154396));
#67446=CARTESIAN_POINT('Ctrl Pts',(16.7502805020365,3.50632200131228,331.548374188722));
#67447=CARTESIAN_POINT('Ctrl Pts',(16.7425333587307,3.40861135090441,331.451849333705));
#67448=CARTESIAN_POINT('Ctrl Pts',(16.7347862154249,3.30706491417161,331.359601022421));
#67449=CARTESIAN_POINT('Ctrl Pts',(16.7270373303968,3.20549564764379,331.267331971759));
#67450=CARTESIAN_POINT('Ctrl Pts',(16.7192884453687,3.10008916804011,331.179341640801));
#67451=CARTESIAN_POINT('Ctrl Pts',(16.7115395603406,2.99125013697079,331.095950092459));
#67452=CARTESIAN_POINT('Ctrl Pts',(16.7037824505659,2.88229558302938,331.012470031466));
#67453=CARTESIAN_POINT('Ctrl Pts',(16.6960253407912,2.76990151045928,330.933598741838));
#67454=CARTESIAN_POINT('Ctrl Pts',(16.6882682310165,2.65450319175973,330.859614043662));
#67455=CARTESIAN_POINT('Ctrl Pts',(16.6805069760903,2.53904320788847,330.785589810429));
#67456=CARTESIAN_POINT('Ctrl Pts',(16.6727457211641,2.42057611646222,330.716457568682));
#67457=CARTESIAN_POINT('Ctrl Pts',(16.664984466238,2.29956215953446,330.652449317496));
#67458=CARTESIAN_POINT('Ctrl Pts',(16.6572107958333,2.17835461971397,330.588338673969));
#67459=CARTESIAN_POINT('Ctrl Pts',(16.6494371254287,2.05459242607519,330.52936856869));
#67460=CARTESIAN_POINT('Ctrl Pts',(16.641663455024,1.92875699328141,330.475723314897));
#67461=CARTESIAN_POINT('Ctrl Pts',(16.6342516508469,1.80877923015725,330.424575260573));
#67462=CARTESIAN_POINT('Ctrl Pts',(16.6268398466697,1.68691717170806,330.378267572696));
#67463=CARTESIAN_POINT('Ctrl Pts',(16.6194280424926,1.56359941462945,330.33691733581));
#67464=CARTESIAN_POINT('Ctrl Pts',(16.6116529637141,1.4342374869328,330.293540400639));
#67465=CARTESIAN_POINT('Ctrl Pts',(16.6038778849357,1.30286474868591,330.255482083691));
#67466=CARTESIAN_POINT('Ctrl Pts',(16.5961028061573,1.16995793220479,330.222931704552));
#67467=CARTESIAN_POINT('Ctrl Pts',(16.5883372951082,1.03721466602261,330.190421380728));
#67468=CARTESIAN_POINT('Ctrl Pts',(16.5805717840592,0.902941453773608,330.163405600792));
#67469=CARTESIAN_POINT('Ctrl Pts',(16.5728062730102,0.767632731889764,330.142024799216));
#67470=CARTESIAN_POINT('Ctrl Pts',(16.565048461488,0.632458168997517,330.120665196767));
#67471=CARTESIAN_POINT('Ctrl Pts',(16.5572906499658,0.496250523279944,330.104929514653));
#67472=CARTESIAN_POINT('Ctrl Pts',(16.5495328384436,0.359516700022947,330.094907666016));
#67473=CARTESIAN_POINT('Ctrl Pts',(16.5417808649206,0.222885773304215,330.084893359139));
#67474=CARTESIAN_POINT('Ctrl Pts',(16.5340288913975,0.0857298454545552,
330.080584355574));
#67475=CARTESIAN_POINT('Ctrl Pts',(16.5262769178745,-0.0514370907015078,
330.08201898253));
#67476=CARTESIAN_POINT('Ctrl Pts',(16.5185282273169,-0.188545936578672,
330.08345300192));
#67477=CARTESIAN_POINT('Ctrl Pts',(16.5107795367593,-0.325665391450322,
330.090625809819));
#67478=CARTESIAN_POINT('Ctrl Pts',(16.5030308462017,-0.462279700181053,
330.103523660702));
#67479=CARTESIAN_POINT('Ctrl Pts',(16.4952837678239,-0.598865585163827,
330.116418828081));
#67480=CARTESIAN_POINT('Ctrl Pts',(16.4875366894461,-0.734946144157236,
330.13503663246));
#67481=CARTESIAN_POINT('Ctrl Pts',(16.4797896110682,-0.870009383243863,
330.159311336642));
#67482=CARTESIAN_POINT('Ctrl Pts',(16.4720424677624,-1.00507375429034,330.183586244268));
#67483=CARTESIAN_POINT('Ctrl Pts',(16.4642953244566,-1.13912040371388,330.213518077117));
#67484=CARTESIAN_POINT('Ctrl Pts',(16.4565481811508,-1.27164658035278,330.248989787721));
#67485=CARTESIAN_POINT('Ctrl Pts',(16.4487992961227,-1.4042025516898,330.28446947312));
#67486=CARTESIAN_POINT('Ctrl Pts',(16.4410504110946,-1.53523699252033,330.325491413601));
#67487=CARTESIAN_POINT('Ctrl Pts',(16.4333015260665,-1.66426176949551,330.371888524993));
#67488=CARTESIAN_POINT('Ctrl Pts',(16.4255444162918,-1.79342349470222,330.418334882757));
#67489=CARTESIAN_POINT('Ctrl Pts',(16.4177873065171,-1.9205709266335,330.470167675753));
#67490=CARTESIAN_POINT('Ctrl Pts',(16.4100301967423,-2.04523488952654,330.527171218439));
#67491=CARTESIAN_POINT('Ctrl Pts',(16.4022689418162,-2.16996546885528,330.584205221995));
#67492=CARTESIAN_POINT('Ctrl Pts',(16.39450768689,-2.29220958662364,330.646415303743));
#67493=CARTESIAN_POINT('Ctrl Pts',(16.3867464319638,-2.41152308647459,330.713539984334));
#67494=CARTESIAN_POINT('Ctrl Pts',(16.3789727615592,-2.53102744904113,330.780772042539));
#67495=CARTESIAN_POINT('Ctrl Pts',(16.3711990911545,-2.64759149309368,330.85293420385));
#67496=CARTESIAN_POINT('Ctrl Pts',(16.3634254207498,-2.76079970460016,330.929721378876));
#67497=CARTESIAN_POINT('Ctrl Pts',(16.3560136165728,-2.86873804662408,331.00293409243));
#67498=CARTESIAN_POINT('Ctrl Pts',(16.3486018123957,-2.97362572156053,331.080350750147));
#67499=CARTESIAN_POINT('Ctrl Pts',(16.3411900082187,-3.07513233225145,331.161674297087));
#67500=CARTESIAN_POINT('Ctrl Pts',(16.3335141690707,-3.18025497142408,331.245894879599));
#67501=CARTESIAN_POINT('Ctrl Pts',(16.3258383299227,-3.28210183978033,331.334587076303));
#67502=CARTESIAN_POINT('Ctrl Pts',(16.3181624907747,-3.38026131157352,331.427463572197));
#67503=CARTESIAN_POINT('Ctrl Pts',(16.3104961427773,-3.47829940949248,331.520225226599));
#67504=CARTESIAN_POINT('Ctrl Pts',(16.30282979478,-3.57265888958396,331.617160617445));
#67505=CARTESIAN_POINT('Ctrl Pts',(16.2951634467827,-3.66295916811724,331.717940708152));
#67506=CARTESIAN_POINT('Ctrl Pts',(16.2875046312394,-3.75317072348035,331.818621778908));
#67507=CARTESIAN_POINT('Ctrl Pts',(16.2798458156961,-3.83933074426663,331.923139738197));
#67508=CARTESIAN_POINT('Ctrl Pts',(16.2721870001528,-3.92109404713248,332.031127396461));
#67509=CARTESIAN_POINT('Ctrl Pts',(16.264533820451,-4.00279718338208,332.139035590568));
#67510=CARTESIAN_POINT('Ctrl Pts',(16.2568806407491,-4.0801097976907,332.250408084321));
#67511=CARTESIAN_POINT('Ctrl Pts',(16.2492274610473,-4.15272605244681,332.364843572797));
#67512=CARTESIAN_POINT('Ctrl Pts',(16.2415772870008,-4.2253137884121,332.479234118694));
#67513=CARTESIAN_POINT('Ctrl Pts',(16.2339271129543,-4.29320861703059,332.59668492898));
#67514=CARTESIAN_POINT('Ctrl Pts',(16.2262769389078,-4.35614744632711,332.716764907339));
#67515=CARTESIAN_POINT('Ctrl Pts',(16.2186280131359,-4.41907600593063,332.836825292316));
#67516=CARTESIAN_POINT('Ctrl Pts',(16.2109790873639,-4.47704998820667,332.959513636374));
#67517=CARTESIAN_POINT('Ctrl Pts',(16.203330161592,-4.5298520481639,333.084373866266));
#67518=CARTESIAN_POINT('Ctrl Pts',(16.1956807279596,-4.582657613983,333.209242386416));
#67519=CARTESIAN_POINT('Ctrl Pts',(16.1880312943272,-4.63029041903972,333.336282708764));
#67520=CARTESIAN_POINT('Ctrl Pts',(16.1803818606948,-4.67258130975759,333.465018903633));
#67521=CARTESIAN_POINT('Ctrl Pts',(16.172726057847,-4.71490741351321,333.593862289256));
#67522=CARTESIAN_POINT('Ctrl Pts',(16.1650702549992,-4.75188259296183,333.724403985612));
#67523=CARTESIAN_POINT('Ctrl Pts',(16.1574144521513,-4.783387564101,333.856152775016));
#67524=CARTESIAN_POINT('Ctrl Pts',(16.1497554281956,-4.81490579066376,333.987956996497));
#67525=CARTESIAN_POINT('Ctrl Pts',(16.1420964042399,-4.84094914721595,334.120968928487));
#67526=CARTESIAN_POINT('Ctrl Pts',(16.1344373802842,-4.86144977132166,334.254688532614));
#67527=CARTESIAN_POINT('Ctrl Pts',(16.126767680111,-4.88197897206121,334.388594533807));
#67528=CARTESIAN_POINT('Ctrl Pts',(16.1190979799378,-4.89694996133167,334.523209778453));
#67529=CARTESIAN_POINT('Ctrl Pts',(16.1114282797645,-4.90634686277453,334.658029936043));
#67530=CARTESIAN_POINT('Ctrl Pts',(16.1048913120252,-4.91435594268563,334.772938602729));
#67531=CARTESIAN_POINT('Ctrl Pts',(16.0983543442858,-4.9183167050879,334.887995953286));
#67532=CARTESIAN_POINT('Ctrl Pts',(16.0918173765464,-4.91824914986108,335.002891779856));
#67533=CARTESIAN_POINT('',(14.34181737647,-4.91824815738865,334.995742671829));
#67534=CARTESIAN_POINT('Ctrl Pts',(16.0918173765088,-4.91824914986069,335.002891780519));
#67535=CARTESIAN_POINT('Ctrl Pts',(16.0821955756541,-4.91814971490646,335.172007616235));
#67536=CARTESIAN_POINT('Ctrl Pts',(16.0725737747994,-4.90932828771645,335.34086422783));
#67537=CARTESIAN_POINT('Ctrl Pts',(16.0629519739447,-4.89186052670427,335.508806102334));
#67538=CARTESIAN_POINT('Ctrl Pts',(16.0551768951664,-4.87774537092409,335.644514721143));
#67539=CARTESIAN_POINT('Ctrl Pts',(16.0474018163881,-4.85795644605174,335.779849972631));
#67540=CARTESIAN_POINT('Ctrl Pts',(16.0396267376098,-4.83251895341018,335.91429952829));
#67541=CARTESIAN_POINT('Ctrl Pts',(16.0318612265609,-4.80711276322274,336.048583635211));
#67542=CARTESIAN_POINT('Ctrl Pts',(16.0240957155119,-4.77607190757694,336.181983834512));
#67543=CARTESIAN_POINT('Ctrl Pts',(16.016330204463,-4.73947341494043,336.313991937408));
#67544=CARTESIAN_POINT('Ctrl Pts',(16.0085723929409,-4.70291120981595,336.445869153885));
#67545=CARTESIAN_POINT('Ctrl Pts',(16.0008145814189,-4.66080243749055,336.576356646528));
#67546=CARTESIAN_POINT('Ctrl Pts',(15.9930567698968,-4.61327527380629,336.704955808984));
#67547=CARTESIAN_POINT('Ctrl Pts',(15.9853047963738,-4.56578387581976,336.833458196492));
#67548=CARTESIAN_POINT('Ctrl Pts',(15.9775528228508,-4.5128823375158,336.960074717139));
#67549=CARTESIAN_POINT('Ctrl Pts',(15.9698008493279,-4.45474872158878,337.084321685826));
#67550=CARTESIAN_POINT('Ctrl Pts',(15.9620521587703,-4.39663972528277,337.208516035847));
#67551=CARTESIAN_POINT('Ctrl Pts',(15.9543034682128,-4.33330322370507,337.330342476512));
#67552=CARTESIAN_POINT('Ctrl Pts',(15.9465547776553,-4.26496540322883,337.449337292363));
#67553=CARTESIAN_POINT('Ctrl Pts',(15.9388076992775,-4.1966418010069,337.56830735035));
#67554=CARTESIAN_POINT('Ctrl Pts',(15.9310606208997,-4.12331914418319,337.684446616628));
#67555=CARTESIAN_POINT('Ctrl Pts',(15.9233135425219,-4.04526938065443,337.797316339001));
#67556=CARTESIAN_POINT('Ctrl Pts',(15.9155663992162,-3.96721896299357,337.91018700733));
#67557=CARTESIAN_POINT('Ctrl Pts',(15.9078192559104,-3.88444158192184,338.019787755602));
#67558=CARTESIAN_POINT('Ctrl Pts',(15.9000721126046,-3.79725205569251,338.125709501543));
#67559=CARTESIAN_POINT('Ctrl Pts',(15.8923232275766,-3.7100429274066,338.231655060942));
#67560=CARTESIAN_POINT('Ctrl Pts',(15.8845743425486,-3.61841992847046,338.333919670413));
#67561=CARTESIAN_POINT('Ctrl Pts',(15.8768254575206,-3.52273736150397,338.432128282038));
#67562=CARTESIAN_POINT('Ctrl Pts',(15.8690683477459,-3.42695323607219,338.530441133298));
#67563=CARTESIAN_POINT('Ctrl Pts',(15.8613112379712,-3.32710120843979,338.624689106506));
#67564=CARTESIAN_POINT('Ctrl Pts',(15.8535541281965,-3.22357196127322,338.714534543249));
#67565=CARTESIAN_POINT('Ctrl Pts',(15.8457928732704,-3.11998739138741,338.804427990522));
#67566=CARTESIAN_POINT('Ctrl Pts',(15.8380316183443,-3.01272199207038,338.889913970127));
#67567=CARTESIAN_POINT('Ctrl Pts',(15.8302703634182,-2.90219775936294,338.970696567109));
#67568=CARTESIAN_POINT('Ctrl Pts',(15.8224966930136,-2.79149672390278,339.051608389919));
#67569=CARTESIAN_POINT('Ctrl Pts',(15.814723022609,-2.67752676290891,339.127801577814));
#67570=CARTESIAN_POINT('Ctrl Pts',(15.8069493522044,-2.56073769729483,339.199024351936));
#67571=CARTESIAN_POINT('Ctrl Pts',(15.7995375480264,-2.44938519076853,339.266931688796));
#67572=CARTESIAN_POINT('Ctrl Pts',(15.7921257438484,-2.33547038327594,339.330320803664));
#67573=CARTESIAN_POINT('Ctrl Pts',(15.7847139396704,-2.21940051954287,339.389014057434));
#67574=CARTESIAN_POINT('Ctrl Pts',(15.776938860892,-2.09764172604811,339.450584042402));
#67575=CARTESIAN_POINT('Ctrl Pts',(15.7691637821135,-1.97312650308235,339.507180783415));
#67576=CARTESIAN_POINT('Ctrl Pts',(15.7613887033351,-1.84629931650026,339.558548222449));
#67577=CARTESIAN_POINT('Ctrl Pts',(15.753623192286,-1.71962819884547,339.609852450579));
#67578=CARTESIAN_POINT('Ctrl Pts',(15.745857681237,-1.59065113716918,339.655940035183));
#67579=CARTESIAN_POINT('Ctrl Pts',(15.7380921701879,-1.45983716278622,339.696600741031));
#67580=CARTESIAN_POINT('Ctrl Pts',(15.7303343586657,-1.32915289083964,339.73722113167));
#67581=CARTESIAN_POINT('Ctrl Pts',(15.7225765471435,-1.19663570153935,339.772425236311));
#67582=CARTESIAN_POINT('Ctrl Pts',(15.7148187356213,-1.06277424690823,339.802051016244));
#67583=CARTESIAN_POINT('Ctrl Pts',(15.7070667620983,-0.929013527266889,
339.831654501838));
#67584=CARTESIAN_POINT('Ctrl Pts',(15.6993147885753,-0.793910935942417,
339.85568793425));
#67585=CARTESIAN_POINT('Ctrl Pts',(15.6915628150523,-0.657969573995112,
339.874039300436));
#67586=CARTESIAN_POINT('Ctrl Pts',(15.6838141244946,-0.522085783295301,
339.892382894808));
#67587=CARTESIAN_POINT('Ctrl Pts',(15.676065433937,-0.385364315034437,339.905049156849));
#67588=CARTESIAN_POINT('Ctrl Pts',(15.6683167433794,-0.248317519857097,
339.911977348465));
#67589=CARTESIAN_POINT('Ctrl Pts',(15.6605696650016,-0.111299238409945,
339.918904098613));
#67590=CARTESIAN_POINT('Ctrl Pts',(15.6528225866237,0.026043845188808,339.920095133272));
#67591=CARTESIAN_POINT('Ctrl Pts',(15.6450755082458,0.163195608243161,339.91554170524));
#67592=CARTESIAN_POINT('Ctrl Pts',(15.63732836494,0.300348520761203,339.910988239045));
#67593=CARTESIAN_POINT('Ctrl Pts',(15.6295812216343,0.437309718877592,339.900690227103));
#67594=CARTESIAN_POINT('Ctrl Pts',(15.6218340783285,0.573564830359344,339.884691028906));
#67595=CARTESIAN_POINT('Ctrl Pts',(15.6140851933004,0.709850574882936,339.86868823375));
#67596=CARTESIAN_POINT('Ctrl Pts',(15.6063363082722,0.845429528759173,339.846981747379));
#67597=CARTESIAN_POINT('Ctrl Pts',(15.5985874232441,0.979794572714952,339.819666550476));
#67598=CARTESIAN_POINT('Ctrl Pts',(15.5908303134694,1.11430223311664,339.792322360941));
#67599=CARTESIAN_POINT('Ctrl Pts',(15.5830732036947,1.24759302614062,339.759357646905));
#67600=CARTESIAN_POINT('Ctrl Pts',(15.57531609392,1.37917158681665,339.720918215413));
#67601=CARTESIAN_POINT('Ctrl Pts',(15.5675548389938,1.51082045886853,339.682458243118));
#67602=CARTESIAN_POINT('Ctrl Pts',(15.5597935840676,1.6407549053409,339.638517849172));
#67603=CARTESIAN_POINT('Ctrl Pts',(15.5520323291415,1.76849771876267,339.589291762487));
#67604=CARTESIAN_POINT('Ctrl Pts',(15.5442586587368,1.89644487905446,339.539986930106));
#67605=CARTESIAN_POINT('Ctrl Pts',(15.5364849883322,2.02219304175565,339.485379664396));
#67606=CARTESIAN_POINT('Ctrl Pts',(15.5287113179275,2.14528705674561,339.425711977373));
#67607=CARTESIAN_POINT('Ctrl Pts',(15.5212995137507,2.26265101571975,339.368821835537));
#67608=CARTESIAN_POINT('Ctrl Pts',(15.5138877095737,2.37760211350707,339.307331930981));
#67609=CARTESIAN_POINT('Ctrl Pts',(15.5064759053969,2.48977058610487,339.241488593768));
#67610=CARTESIAN_POINT('Ctrl Pts',(15.4987008266184,2.60743676968059,339.17241807846));
#67611=CARTESIAN_POINT('Ctrl Pts',(15.49092574784,2.7224125084653,339.098338315135));
#67612=CARTESIAN_POINT('Ctrl Pts',(15.4831506690616,2.83424195182712,339.019484496923));
#67613=CARTESIAN_POINT('Ctrl Pts',(15.4753851580126,2.94593378193949,338.940727713354));
#67614=CARTESIAN_POINT('Ctrl Pts',(15.4676196469635,3.0544867038435,338.85720878712));
#67615=CARTESIAN_POINT('Ctrl Pts',(15.4598541359145,3.15947010649189,338.769208366313));
#67616=CARTESIAN_POINT('Ctrl Pts',(15.4520963243923,3.26434941779098,338.681295198179));
#67617=CARTESIAN_POINT('Ctrl Pts',(15.4443385128701,3.36566595539473,338.588909627599));
#67618=CARTESIAN_POINT('Ctrl Pts',(15.4365807013479,3.4630190198484,338.492374884039));
#67619=CARTESIAN_POINT('Ctrl Pts',(15.4288287278249,3.56029882303368,338.395912785936));
#67620=CARTESIAN_POINT('Ctrl Pts',(15.4210767543019,3.65362081343013,338.29530800392));
#67621=CARTESIAN_POINT('Ctrl Pts',(15.4133247807789,3.74261854002876,338.190922989721));
#67622=CARTESIAN_POINT('Ctrl Pts',(15.4055760902212,3.83157857603734,338.086582182638));
#67623=CARTESIAN_POINT('Ctrl Pts',(15.3978273996636,3.91621773756256,337.978464624334));
#67624=CARTESIAN_POINT('Ctrl Pts',(15.3900787091059,3.99620768631268,337.866968292527));
#67625=CARTESIAN_POINT('Ctrl Pts',(15.3823316307281,4.07618099248586,337.755495158463));
#67626=CARTESIAN_POINT('Ctrl Pts',(15.3745845523503,4.15150678221994,337.640644966575));
#67627=CARTESIAN_POINT('Ctrl Pts',(15.3668374739724,4.22189839619979,337.522847001835));
#67628=CARTESIAN_POINT('Ctrl Pts',(15.3590903306666,4.29229060012918,337.405048049834));
#67629=CARTESIAN_POINT('Ctrl Pts',(15.3513431873609,4.35774834532099,337.284301611237));
#67630=CARTESIAN_POINT('Ctrl Pts',(15.343596044055,4.41802973736865,337.161063696939));
#67631=CARTESIAN_POINT('Ctrl Pts',(15.3358471590269,4.47832468195305,337.037798076141));
#67632=CARTESIAN_POINT('Ctrl Pts',(15.3280982739988,4.53344078593731,336.912040216083));
#67633=CARTESIAN_POINT('Ctrl Pts',(15.3203493889707,4.58318348926699,336.784267963679));
#67634=CARTESIAN_POINT('Ctrl Pts',(15.3125922791959,4.63297899001591,336.656360092486));
#67635=CARTESIAN_POINT('Ctrl Pts',(15.3048351694211,4.67738955504035,336.526433922717));
#67636=CARTESIAN_POINT('Ctrl Pts',(15.2970780596464,4.7162697261879,336.394984921905));
#67637=CARTESIAN_POINT('Ctrl Pts',(15.2893168047202,4.75517067365573,336.263465678951));
#67638=CARTESIAN_POINT('Ctrl Pts',(15.2815555497941,4.78853524358274,336.130422362419));
#67639=CARTESIAN_POINT('Ctrl Pts',(15.2737942948679,4.8162689433202,335.996361645242));
#67640=CARTESIAN_POINT('Ctrl Pts',(15.2660206244632,4.84404700793884,335.862086474608));
#67641=CARTESIAN_POINT('Ctrl Pts',(15.2582469540585,4.86617613947431,335.726791037033));
#67642=CARTESIAN_POINT('Ctrl Pts',(15.2504732836538,4.88261354314653,335.590989044553));
#67643=CARTESIAN_POINT('Ctrl Pts',(15.2430614794768,4.89828578172304,335.461508667497));
#67644=CARTESIAN_POINT('Ctrl Pts',(15.2356496752998,4.90878424405759,335.331568121346));
#67645=CARTESIAN_POINT('Ctrl Pts',(15.2282378711228,4.914115973838,335.201611651871));
#67646=CARTESIAN_POINT('Ctrl Pts',(15.2204627923444,4.9197090275774,335.065285628706));
#67647=CARTESIAN_POINT('Ctrl Pts',(15.2126877135659,4.91963374373762,334.928511266431));
#67648=CARTESIAN_POINT('Ctrl Pts',(15.2049126347875,4.91384121430612,334.791799176067));
#67649=CARTESIAN_POINT('Ctrl Pts',(15.1971471237385,4.90805581295086,334.655255318633));
#67650=CARTESIAN_POINT('Ctrl Pts',(15.1893816126895,4.89656718089003,334.518773967429));
#67651=CARTESIAN_POINT('Ctrl Pts',(15.1816161016405,4.87937829274619,334.382869107257));
#67652=CARTESIAN_POINT('Ctrl Pts',(15.1738582901183,4.86220644743501,334.247098997151));
#67653=CARTESIAN_POINT('Ctrl Pts',(15.1661004785962,4.83934564221326,334.111904625863));
#67654=CARTESIAN_POINT('Ctrl Pts',(15.158342667074,4.8108508461696,333.977797868125));
#67655=CARTESIAN_POINT('Ctrl Pts',(15.150590693551,4.7823774933636,333.843792029976));
#67656=CARTESIAN_POINT('Ctrl Pts',(15.142838720028,4.7482786696759,333.710872557064));
#67657=CARTESIAN_POINT('Ctrl Pts',(15.135086746505,4.70866086083099,333.579543749291));
#67658=CARTESIAN_POINT('Ctrl Pts',(15.1273380559474,4.66905983015165,333.448270559346));
#67659=CARTESIAN_POINT('Ctrl Pts',(15.1195893653898,4.62394457568195,333.318587068139));
#67660=CARTESIAN_POINT('Ctrl Pts',(15.1118406748322,4.57347208268703,333.190984750926));
#67661=CARTESIAN_POINT('Ctrl Pts',(15.1040935964544,4.52301009091583,333.063408982441));
#67662=CARTESIAN_POINT('Ctrl Pts',(15.0963465180766,4.46719322135376,332.937913889915));
#67663=CARTESIAN_POINT('Ctrl Pts',(15.0885994396988,4.40622734108901,332.814972842013));
#67664=CARTESIAN_POINT('Ctrl Pts',(15.080852296393,4.34526094987146,332.692030763747));
#67665=CARTESIAN_POINT('Ctrl Pts',(15.0731051530872,4.27914563553143,332.571643122982));
#67666=CARTESIAN_POINT('Ctrl Pts',(15.0653580097814,4.20813396441528,332.454260107545));
#67667=CARTESIAN_POINT('Ctrl Pts',(15.0576091247533,4.13710632836795,332.336850701915));
#67668=CARTESIAN_POINT('Ctrl Pts',(15.0498602397253,4.06118034734689,332.222447600163));
#67669=CARTESIAN_POINT('Ctrl Pts',(15.0421113546972,3.9806525654066,332.111473002373));
#67670=CARTESIAN_POINT('Ctrl Pts',(15.0343542449225,3.90003931044644,332.000380614998));
#67671=CARTESIAN_POINT('Ctrl Pts',(15.0265971351478,3.81481472744786,331.892724317787));
#67672=CARTESIAN_POINT('Ctrl Pts',(15.0188400253731,3.7253167498758,331.788894555516));
#67673=CARTESIAN_POINT('Ctrl Pts',(15.0110787704469,3.63577094744606,331.685009309939));
#67674=CARTESIAN_POINT('Ctrl Pts',(15.0033175155208,3.54194746746658,331.584954958687));
#67675=CARTESIAN_POINT('Ctrl Pts',(14.9955562605946,3.44422124662003,331.489085152438));
#67676=CARTESIAN_POINT('Ctrl Pts',(14.98778259019,3.34633869566916,331.393061985743));
#67677=CARTESIAN_POINT('Ctrl Pts',(14.9800089197853,3.24454121865485,331.301237002409));
#67678=CARTESIAN_POINT('Ctrl Pts',(14.9722352493806,3.13923764827562,331.213924188537));
#67679=CARTESIAN_POINT('Ctrl Pts',(14.9648234452034,3.03883598442941,331.130675807154));
#67680=CARTESIAN_POINT('Ctrl Pts',(14.9574116410261,2.93524752737839,331.05152914069));
#67681=CARTESIAN_POINT('Ctrl Pts',(14.9499998368489,2.82884966461261,330.976718672834));
#67682=CARTESIAN_POINT('Ctrl Pts',(14.9422247580704,2.71723692565213,330.898241521102));
#67683=CARTESIAN_POINT('Ctrl Pts',(14.9344496792919,2.60217970605613,330.82428837335));
#67684=CARTESIAN_POINT('Ctrl Pts',(14.9266746005135,2.48408092259265,330.755176678293));
#67685=CARTESIAN_POINT('Ctrl Pts',(14.9189090894644,2.36612746720076,330.686150029576));
#67686=CARTESIAN_POINT('Ctrl Pts',(14.9111435784154,2.24514022924499,330.62195317494));
#67687=CARTESIAN_POINT('Ctrl Pts',(14.9033780673664,2.12155303925051,330.562861759631));
#67688=CARTESIAN_POINT('Ctrl Pts',(14.8956202558442,1.99808838631481,330.503828933632));
#67689=CARTESIAN_POINT('Ctrl Pts',(14.887862444322,1.87202926179428,330.449891640701));
#67690=CARTESIAN_POINT('Ctrl Pts',(14.8801046327997,1.74383585899968,330.401280660948));
#67691=CARTESIAN_POINT('Ctrl Pts',(14.8723526592767,1.61573892580593,330.352706262499));
#67692=CARTESIAN_POINT('Ctrl Pts',(14.8646006857537,1.48551127523392,330.309450337095));
#67693=CARTESIAN_POINT('Ctrl Pts',(14.8568487122307,1.35363460936395,330.27169624423));
#67694=CARTESIAN_POINT('Ctrl Pts',(14.849100021673,1.2218137933401,330.233958140245));
#67695=CARTESIAN_POINT('Ctrl Pts',(14.8413513311153,1.08834572600145,330.201717341892));
#67696=CARTESIAN_POINT('Ctrl Pts',(14.8336026405576,0.953728653109309,330.175107802371));
#67697=CARTESIAN_POINT('Ctrl Pts',(14.8258555621798,0.819139588423713,330.148503799188));
#67698=CARTESIAN_POINT('Ctrl Pts',(14.818108483802,0.683402376906288,330.127528800131));
#67699=CARTESIAN_POINT('Ctrl Pts',(14.8103614054241,0.547026490860267,330.11226585412));
#67700=CARTESIAN_POINT('Ctrl Pts',(14.8026142621183,0.410649461852968,330.097002780192));
#67701=CARTESIAN_POINT('Ctrl Pts',(14.7948671188124,0.273634136089762,330.08745189827));
#67702=CARTESIAN_POINT('Ctrl Pts',(14.7871199755066,0.136495764261796,330.08364444239));
#67703=CARTESIAN_POINT('Ctrl Pts',(14.7793710904785,-0.000673439183687147,
330.079836130514));
#67704=CARTESIAN_POINT('Ctrl Pts',(14.7716222054503,-0.137965353093567,
330.081773824958));
#67705=CARTESIAN_POINT('Ctrl Pts',(14.7638733204222,-0.27486446340625,330.089436632192));
#67706=CARTESIAN_POINT('Ctrl Pts',(14.7561162106475,-0.411908879849051,
330.097107572809));
#67707=CARTESIAN_POINT('Ctrl Pts',(14.7483591008727,-0.548559268966453,
330.110515743102));
#67708=CARTESIAN_POINT('Ctrl Pts',(14.740601991098,-0.684304422229046,330.129588259683));
#67709=CARTESIAN_POINT('Ctrl Pts',(14.7328407361718,-0.820122113361162,
330.148670968007));
#67710=CARTESIAN_POINT('Ctrl Pts',(14.7250794812455,-0.955033220502945,
330.173423983378));
#67711=CARTESIAN_POINT('Ctrl Pts',(14.7173182263193,-1.08853745149997,330.203723394217));
#67712=CARTESIAN_POINT('Ctrl Pts',(14.7095445559147,-1.22225524575765,330.234071274238));
#67713=CARTESIAN_POINT('Ctrl Pts',(14.70177088551,-1.35456128919484,330.269983177016));
#67714=CARTESIAN_POINT('Ctrl Pts',(14.6939972151054,-1.48497030136749,330.311285222307));
#67715=CARTESIAN_POINT('Ctrl Pts',(14.6865854109286,-1.60930874264362,330.350664647452));
#67716=CARTESIAN_POINT('Ctrl Pts',(14.6791736067518,-1.7319225210002,330.394943588288));
#67717=CARTESIAN_POINT('Ctrl Pts',(14.671761802575,-1.85241022807443,330.443931584203));
#67718=CARTESIAN_POINT('Ctrl Pts',(14.6639867237966,-1.97880339659117,330.495320627727));
#67719=CARTESIAN_POINT('Ctrl Pts',(14.6562116450182,-2.10325623976096,330.552054406644));
#67720=CARTESIAN_POINT('Ctrl Pts',(14.6484365662398,-2.22528376680622,330.613965889361));
#67721=CARTESIAN_POINT('Ctrl Pts',(14.6406710551908,-2.34716113121096,330.675801186057));
#67722=CARTESIAN_POINT('Ctrl Pts',(14.6329055441418,-2.46661877255756,330.742801333945));
#67723=CARTESIAN_POINT('Ctrl Pts',(14.6251400330928,-2.58319012428785,330.814750683139));
#67724=CARTESIAN_POINT('Ctrl Pts',(14.6173822215707,-2.69964589518328,330.886628694345));
#67725=CARTESIAN_POINT('Ctrl Pts',(14.6096244100485,-2.81322074105874,330.963445937381));
#67726=CARTESIAN_POINT('Ctrl Pts',(14.6018665985264,-2.92347155699022,331.044940314234));
#67727=CARTESIAN_POINT('Ctrl Pts',(14.5941146250034,-3.03363940568646,331.126373363985));
#67728=CARTESIAN_POINT('Ctrl Pts',(14.5863626514804,-3.14048789036884,331.212476310374));
#67729=CARTESIAN_POINT('Ctrl Pts',(14.5786106779574,-3.24360214349043,331.30294330619));
#67730=CARTESIAN_POINT('Ctrl Pts',(14.5708619873999,-3.34667272766474,331.39337198918));
#67731=CARTESIAN_POINT('Ctrl Pts',(14.5631132968423,-3.44601193246008,331.488160788454));
#67732=CARTESIAN_POINT('Ctrl Pts',(14.5553646062847,-3.54123748440004,331.586963208288));
#67733=CARTESIAN_POINT('Ctrl Pts',(14.5476175279069,-3.63644322386857,331.685745071453));
#67734=CARTESIAN_POINT('Ctrl Pts',(14.539870449529,-3.72753674180896,331.788538612908));
#67735=CARTESIAN_POINT('Ctrl Pts',(14.5321233711512,-3.8141724959158,331.894960349062));
#67736=CARTESIAN_POINT('Ctrl Pts',(14.5243762278455,-3.90080897611358,332.001382977131));
#67737=CARTESIAN_POINT('Ctrl Pts',(14.5166290845397,-3.98298737118907,332.111433557421));
#67738=CARTESIAN_POINT('Ctrl Pts',(14.508881941234,-4.06040258406053,332.22469570716));
#67739=CARTESIAN_POINT('Ctrl Pts',(14.5011330562059,-4.13783520151542,332.337983320636));
#67740=CARTESIAN_POINT('Ctrl Pts',(14.4933841711778,-4.21050228534343,332.454483617685));
#67741=CARTESIAN_POINT('Ctrl Pts',(14.4856352861498,-4.27814243112122,332.573751784846));
#67742=CARTESIAN_POINT('Ctrl Pts',(14.4778781763751,-4.34585437084869,332.693146544472));
#67743=CARTESIAN_POINT('Ctrl Pts',(14.4701210666004,-4.40852852094766,332.815314702294));
#67744=CARTESIAN_POINT('Ctrl Pts',(14.4623639568257,-4.46594952634627,332.93978693077));
#67745=CARTESIAN_POINT('Ctrl Pts',(14.4546027018995,-4.52340121569416,333.064325673224));
#67746=CARTESIAN_POINT('Ctrl Pts',(14.4468414469735,-4.57559401825847,333.191170578366));
#67747=CARTESIAN_POINT('Ctrl Pts',(14.4390801920473,-4.62236139713883,333.319833884183));
#67748=CARTESIAN_POINT('Ctrl Pts',(14.4313065216427,-4.66920358858396,333.448703009357));
#67749=CARTESIAN_POINT('Ctrl Pts',(14.423532851238,-4.71060289521525,333.579395975125));
#67750=CARTESIAN_POINT('Ctrl Pts',(14.4157591808334,-4.74644292354394,333.711410602232));
#67751=CARTESIAN_POINT('Ctrl Pts',(14.408347376656,-4.78061458993301,333.837279916693));
#67752=CARTESIAN_POINT('Ctrl Pts',(14.4009355724785,-4.80973283498304,333.964350334385));
#67753=CARTESIAN_POINT('Ctrl Pts',(14.3935237683011,-4.83374059598813,334.092181233287));
#67754=CARTESIAN_POINT('Ctrl Pts',(14.3819320562446,-4.87128760155276,334.292102728315));
#67755=CARTESIAN_POINT('Ctrl Pts',(14.370340344188,-4.89644018138022,334.49441954545));
#67756=CARTESIAN_POINT('Ctrl Pts',(14.3587486321315,-4.90896216907168,334.697884980309));
#67757=CARTESIAN_POINT('Ctrl Pts',(14.3531048802573,-4.91505885187039,334.796947864525));
#67758=CARTESIAN_POINT('Ctrl Pts',(14.347461128383,-4.91816206293123,334.89628267684));
#67759=CARTESIAN_POINT('Ctrl Pts',(14.3418173765088,-4.91824815738806,334.995742671145));
#67760=CARTESIAN_POINT('',(12.5918173765377,-4.91824995487103,334.99933373343));
#67761=CARTESIAN_POINT('Ctrl Pts',(14.34181737647,-4.91824815738865,334.995742671829));
#67762=CARTESIAN_POINT('Ctrl Pts',(14.334169784482,-4.91836482006042,335.130516395504));
#67763=CARTESIAN_POINT('Ctrl Pts',(14.326522192494,-4.91293755736548,335.265479041663));
#67764=CARTESIAN_POINT('Ctrl Pts',(14.3188746005059,-4.9019465099734,335.400129323919));
#67765=CARTESIAN_POINT('Ctrl Pts',(14.3112337740706,-4.89096518597019,335.534660485857));
#67766=CARTESIAN_POINT('Ctrl Pts',(14.3035929476353,-4.87442990024653,335.668879433724));
#67767=CARTESIAN_POINT('Ctrl Pts',(14.2959521212,-4.85237284976637,335.802284730847));
#67768=CARTESIAN_POINT('Ctrl Pts',(14.2883157222692,-4.83032858032385,335.935612725788));
#67769=CARTESIAN_POINT('Ctrl Pts',(14.2806793233384,-4.8027689747445,336.068127610749));
#67770=CARTESIAN_POINT('Ctrl Pts',(14.2730429244076,-4.76977803608156,336.199333376928));
#67771=CARTESIAN_POINT('Ctrl Pts',(14.2654087960481,-4.73679690679058,336.330500130996));
#67772=CARTESIAN_POINT('Ctrl Pts',(14.2577746676886,-4.69838775293967,336.460358149181));
#67773=CARTESIAN_POINT('Ctrl Pts',(14.2501405393291,-4.65468552394845,336.588422404666));
#67774=CARTESIAN_POINT('Ctrl Pts',(14.2425069150414,-4.61098618055987,336.716478204231));
#67775=CARTESIAN_POINT('Ctrl Pts',(14.2348732907536,-4.56199458734832,336.842740094793));
#67776=CARTESIAN_POINT('Ctrl Pts',(14.2272396664659,-4.50789514943345,336.96673953136));
#67777=CARTESIAN_POINT('Ctrl Pts',(14.2196047803676,-4.4537867690765,337.090759464587));
#67778=CARTESIAN_POINT('Ctrl Pts',(14.2119698942693,-4.39456902696439,337.21251583062));
#67779=CARTESIAN_POINT('Ctrl Pts',(14.204335008171,-4.33047368489916,337.331561864265));
#67780=CARTESIAN_POINT('Ctrl Pts',(14.196692498292,-4.26631434072249,337.450726770784));
#67781=CARTESIAN_POINT('Ctrl Pts',(14.189049988413,-4.19726786124331,337.567175584188));
#67782=CARTESIAN_POINT('Ctrl Pts',(14.181407478534,-4.12361119678431,337.680487597482));
#67783=CARTESIAN_POINT('Ctrl Pts',(14.1737610855969,-4.04991710834897,337.793857183111));
#67784=CARTESIAN_POINT('Ctrl Pts',(14.1661146926598,-3.97160840464576,337.904086466819));
#67785=CARTESIAN_POINT('Ctrl Pts',(14.1584682997227,-3.88900346642052,338.010786458829));
#67786=CARTESIAN_POINT('Ctrl Pts',(14.1508099918539,-3.80626980970002,338.117652715263));
#67787=CARTESIAN_POINT('Ctrl Pts',(14.1431516839851,-3.71922680601404,338.220978386607));
#67788=CARTESIAN_POINT('Ctrl Pts',(14.1354933761164,-3.62823138199011,338.320409628531));
#67789=CARTESIAN_POINT('Ctrl Pts',(14.1287574954199,-3.54819616655459,338.407864585237));
#67790=CARTESIAN_POINT('Ctrl Pts',(14.1220216147235,-3.4651039971073,338.492307206725));
#67791=CARTESIAN_POINT('Ctrl Pts',(14.1152857340271,-3.37921856485625,338.573522765204));
#67792=CARTESIAN_POINT('Ctrl Pts',(14.1075106552484,-3.28008290141734,338.667268096168));
#67793=CARTESIAN_POINT('Ctrl Pts',(14.0997355764698,-3.17688664381494,338.7570331465));
#67794=CARTESIAN_POINT('Ctrl Pts',(14.0919604976912,-3.06998274485364,338.842445706682));
#67795=CARTESIAN_POINT('Ctrl Pts',(14.084194986642,-2.96321039794615,338.927753161271));
#67796=CARTESIAN_POINT('Ctrl Pts',(14.0764294755928,-2.85273979018041,339.008718540995));
#67797=CARTESIAN_POINT('Ctrl Pts',(14.0686639645436,-2.73896049078447,339.085006547415));
#67798=CARTESIAN_POINT('Ctrl Pts',(14.0609061530213,-2.62529400389491,339.161218914054));
#67799=CARTESIAN_POINT('Ctrl Pts',(14.0531483414989,-2.50832567647116,339.23276292026));
#67800=CARTESIAN_POINT('Ctrl Pts',(14.0453905299765,-2.38847763202022,339.29934386434));
#67801=CARTESIAN_POINT('Ctrl Pts',(14.0376385564533,-2.26871977702333,339.365874704148));
#67802=CARTESIAN_POINT('Ctrl Pts',(14.0298865829301,-2.14608685877421,339.427449726832));
#67803=CARTESIAN_POINT('Ctrl Pts',(14.0221346094069,-2.02102912007301,339.483818055889));
#67804=CARTESIAN_POINT('Ctrl Pts',(14.0143859188492,-1.89602434339856,339.540162512925));
#67805=CARTESIAN_POINT('Ctrl Pts',(14.0066372282914,-1.76859714433594,339.591304501714));
#67806=CARTESIAN_POINT('Ctrl Pts',(13.9988885377336,-1.63922125794991,339.637039651543));
#67807=CARTESIAN_POINT('Ctrl Pts',(13.9911414593556,-1.5098722892976,339.682765285793));
#67808=CARTESIAN_POINT('Ctrl Pts',(13.9833943809775,-1.37857580806597,339.723086188472));
#67809=CARTESIAN_POINT('Ctrl Pts',(13.9756473025995,-1.24582399588696,339.757846743409));
#67810=CARTESIAN_POINT('Ctrl Pts',(13.9679001592936,-1.11307107112008,339.792607589674));
#67811=CARTESIAN_POINT('Ctrl Pts',(13.9601530159876,-0.97886316920421,339.821807896238));
#67812=CARTESIAN_POINT('Ctrl Pts',(13.9524058726817,-0.843705658329049,
339.845342487854));
#67813=CARTESIAN_POINT('Ctrl Pts',(13.9446569876534,-0.708517761175785,
339.868882370546));
#67814=CARTESIAN_POINT('Ctrl Pts',(13.9369081026251,-0.572380215242268,
339.886753936584));
#67815=CARTESIAN_POINT('Ctrl Pts',(13.9291592175968,-0.43580616291851,339.898903555987));
#67816=CARTESIAN_POINT('Ctrl Pts',(13.9214021078219,-0.299087149484731,
339.911066071122));
#67817=CARTESIAN_POINT('Ctrl Pts',(13.913644998047,-0.161931094102431,339.917494472878));
#67818=CARTESIAN_POINT('Ctrl Pts',(13.9058878882721,-0.0248543723207421,
339.918187198824));
#67819=CARTESIAN_POINT('Ctrl Pts',(13.8981266333458,0.112295598878295,339.918880294941));
#67820=CARTESIAN_POINT('Ctrl Pts',(13.8903653784194,0.2493657615929,339.913831622414));
#67821=CARTESIAN_POINT('Ctrl Pts',(13.8826041234931,0.385843187537344,339.903091687612));
#67822=CARTESIAN_POINT('Ctrl Pts',(13.8748304530883,0.522538932885219,339.892334572415));
#67823=CARTESIAN_POINT('Ctrl Pts',(13.8670567826835,0.658639658458579,339.875868049097));
#67824=CARTESIAN_POINT('Ctrl Pts',(13.8592831122787,0.793640088523946,339.853794234657));
#67825=CARTESIAN_POINT('Ctrl Pts',(13.8518713081035,0.92235621605493,339.832747961595));
#67826=CARTESIAN_POINT('Ctrl Pts',(13.8444595039283,1.0500718983481,339.806604745773));
#67827=CARTESIAN_POINT('Ctrl Pts',(13.8370476997531,1.17636246605466,339.7754952006));
#67828=CARTESIAN_POINT('Ctrl Pts',(13.8292726209747,1.30884291071678,339.74286088394));
#67829=CARTESIAN_POINT('Ctrl Pts',(13.8214975421965,1.44017367297856,339.70465796878));
#67830=CARTESIAN_POINT('Ctrl Pts',(13.8137224634181,1.56985075090098,339.660981836737));
#67831=CARTESIAN_POINT('Ctrl Pts',(13.8059569523693,1.6993682529232,339.617359450956));
#67832=CARTESIAN_POINT('Ctrl Pts',(13.7981914413203,1.82723575271371,339.568277372861));
#67833=CARTESIAN_POINT('Ctrl Pts',(13.7904259302715,1.95296047239978,339.513881750306));
#67834=CARTESIAN_POINT('Ctrl Pts',(13.7826681187493,2.07856053566083,339.459540061168));
#67835=CARTESIAN_POINT('Ctrl Pts',(13.7749103072272,2.20202169041072,339.399895466182));
#67836=CARTESIAN_POINT('Ctrl Pts',(13.7671524957051,2.3228676804586,339.335143458016));
#67837=CARTESIAN_POINT('Ctrl Pts',(13.7594005221822,2.44362273006622,339.27044017779));
#67838=CARTESIAN_POINT('Ctrl Pts',(13.7516485486593,2.56176618902336,339.200637318527));
#67839=CARTESIAN_POINT('Ctrl Pts',(13.7438965751364,2.67684343771271,339.125977735334));
#67840=CARTESIAN_POINT('Ctrl Pts',(13.7361478845789,2.79187195111922,339.051349770519));
#67841=CARTESIAN_POINT('Ctrl Pts',(13.7283991940213,2.90383650973961,338.971869384951));
#67842=CARTESIAN_POINT('Ctrl Pts',(13.7206505034638,3.01230888865644,338.887824355835));
#67843=CARTESIAN_POINT('Ctrl Pts',(13.7129034250861,3.12075869898872,338.803796812989));
#67844=CARTESIAN_POINT('Ctrl Pts',(13.7051563467084,3.22571746604281,338.71520675489));
#67845=CARTESIAN_POINT('Ctrl Pts',(13.6974092683307,3.32678798113983,338.622383854735));
#67846=CARTESIAN_POINT('Ctrl Pts',(13.689662125025,3.42785934330497,338.529560176634));
#67847=CARTESIAN_POINT('Ctrl Pts',(13.6819149817193,3.52504210062894,338.432503850113));
#67848=CARTESIAN_POINT('Ctrl Pts',(13.6741678384136,3.6179743252772,338.331582933702));
#67849=CARTESIAN_POINT('Ctrl Pts',(13.6664189533856,3.71092744306256,338.230639328127));
#67850=CARTESIAN_POINT('Ctrl Pts',(13.6586700683576,3.79962786189173,338.125829691243));
#67851=CARTESIAN_POINT('Ctrl Pts',(13.6509211833296,3.88375279237792,338.017556513174));
#67852=CARTESIAN_POINT('Ctrl Pts',(13.643164073555,3.96796701393473,337.909168412834));
#67853=CARTESIAN_POINT('Ctrl Pts',(13.6354069637804,4.04759580569605,337.797309736825));
#67854=CARTESIAN_POINT('Ctrl Pts',(13.6276498540057,4.12235841333991,337.682413870838));
#67855=CARTESIAN_POINT('Ctrl Pts',(13.6198885990797,4.19716097173069,337.567456608175));
#67856=CARTESIAN_POINT('Ctrl Pts',(13.6121273441536,4.26709196542435,337.449459257694));
#67857=CARTESIAN_POINT('Ctrl Pts',(13.6043660892276,4.33191629137552,337.328880483626));
#67858=CARTESIAN_POINT('Ctrl Pts',(13.596592418823,4.39684431512211,337.208108822817));
#67859=CARTESIAN_POINT('Ctrl Pts',(13.5888187484184,4.45664917643405,337.08474783849));
#67860=CARTESIAN_POINT('Ctrl Pts',(13.5810450780138,4.51114331398031,336.959277689158));
#67861=CARTESIAN_POINT('Ctrl Pts',(13.5736332738356,4.56310073632166,336.839648205443));
#67862=CARTESIAN_POINT('Ctrl Pts',(13.5662214696574,4.61023063243016,336.718101769282));
#67863=CARTESIAN_POINT('Ctrl Pts',(13.5588096654792,4.65241302495513,336.595066176598));
#67864=CARTESIAN_POINT('Ctrl Pts',(13.5510345867012,4.69666290218368,336.466000243039));
#67865=CARTESIAN_POINT('Ctrl Pts',(13.5432595079232,4.7356078670183,336.334887613764));
#67866=CARTESIAN_POINT('Ctrl Pts',(13.5354844291451,4.76905538352588,336.202203731221));
#67867=CARTESIAN_POINT('Ctrl Pts',(13.5277189180965,4.80246174073503,336.069683124643));
#67868=CARTESIAN_POINT('Ctrl Pts',(13.519953407048,4.83038401531723,335.935595487355));
#67869=CARTESIAN_POINT('Ctrl Pts',(13.5121878959994,4.85267843573541,335.800434295772));
#67870=CARTESIAN_POINT('Ctrl Pts',(13.5044300844776,4.87495075117082,335.665407116904));
#67871=CARTESIAN_POINT('Ctrl Pts',(13.4966722729558,4.89160625382082,335.5293088852));
#67872=CARTESIAN_POINT('Ctrl Pts',(13.488914461434,4.90255160808747,335.39264588695));
#67873=CARTESIAN_POINT('Ctrl Pts',(13.4811624879114,4.91348872562795,335.25608573194));
#67874=CARTESIAN_POINT('Ctrl Pts',(13.4734105143888,4.91872421680874,335.118962044394));
#67875=CARTESIAN_POINT('Ctrl Pts',(13.4656585408661,4.91821628290792,334.981788546479));
#67876=CARTESIAN_POINT('Ctrl Pts',(13.4579098503089,4.91770856411742,334.844673141622));
#67877=CARTESIAN_POINT('Ctrl Pts',(13.4501611597518,4.91146225945038,334.70750835841));
#67878=CARTESIAN_POINT('Ctrl Pts',(13.4424124691946,4.89948762982278,334.57081003307));
#67879=CARTESIAN_POINT('Ctrl Pts',(13.4346653908171,4.88751549161688,334.434140148958));
#67880=CARTESIAN_POINT('Ctrl Pts',(13.4269183124397,4.86981743316448,334.297936918816));
#67881=CARTESIAN_POINT('Ctrl Pts',(13.4191712340623,4.84645573128148,334.16271276898));
#67882=CARTESIAN_POINT('Ctrl Pts',(13.4114240907569,4.82309383360491,334.027487485835));
#67883=CARTESIAN_POINT('Ctrl Pts',(13.4036769474515,4.79406826436447,333.893241684531));
#67884=CARTESIAN_POINT('Ctrl Pts',(13.3959298041461,4.75949267191243,333.760478895496));
#67885=CARTESIAN_POINT('Ctrl Pts',(13.3881809191184,4.724909306133,333.627686258566));
#67886=CARTESIAN_POINT('Ctrl Pts',(13.3804320340907,4.68477353272363,333.496377675542));
#67887=CARTESIAN_POINT('Ctrl Pts',(13.372683149063,4.6392491343566,333.367042397405));
#67888=CARTESIAN_POINT('Ctrl Pts',(13.3649260392887,4.59367641592292,333.237569841469));
#67889=CARTESIAN_POINT('Ctrl Pts',(13.3571689295144,4.54270377719256,333.110075143636));
#67890=CARTESIAN_POINT('Ctrl Pts',(13.3494118197401,4.48654372916801,332.985028926073));
#67891=CARTESIAN_POINT('Ctrl Pts',(13.3416505648143,4.43035367100932,332.859915887809));
#67892=CARTESIAN_POINT('Ctrl Pts',(13.3338893098885,4.36897085495944,332.73725428627));
#67893=CARTESIAN_POINT('Ctrl Pts',(13.3261280549627,4.30265375380793,332.617490034157));
#67894=CARTESIAN_POINT('Ctrl Pts',(13.3183543845584,4.23623056690736,332.497534198272));
#67895=CARTESIAN_POINT('Ctrl Pts',(13.3105807141541,4.16485752546075,332.380485307445));
#67896=CARTESIAN_POINT('Ctrl Pts',(13.3028070437499,4.08883690480455,332.266760927323));
#67897=CARTESIAN_POINT('Ctrl Pts',(13.2953952395683,4.01635506228222,332.158330444386));
#67898=CARTESIAN_POINT('Ctrl Pts',(13.2879834353868,3.9396487620986,332.052922158287));
#67899=CARTESIAN_POINT('Ctrl Pts',(13.2805716312053,3.85901282034596,331.950868465463));
#67900=CARTESIAN_POINT('Ctrl Pts',(13.2727965524257,3.7744246709235,331.8438128172));
#67901=CARTESIAN_POINT('Ctrl Pts',(13.265021473646,3.68524461891527,331.740110598454));
#67902=CARTESIAN_POINT('Ctrl Pts',(13.2572463948663,3.59176828177825,331.64018100599));
#67903=CARTESIAN_POINT('Ctrl Pts',(13.2494808838161,3.49840697322505,331.540374383251));
#67904=CARTESIAN_POINT('Ctrl Pts',(13.2417153727659,3.40076016332989,331.444331432359));
#67905=CARTESIAN_POINT('Ctrl Pts',(13.2339498617157,3.29916502390904,331.352440102272));
#67906=CARTESIAN_POINT('Ctrl Pts',(13.2261920501923,3.19767061636477,331.260639882706));
#67907=CARTESIAN_POINT('Ctrl Pts',(13.2184342386689,3.09223595794855,331.172983352695));
#67908=CARTESIAN_POINT('Ctrl Pts',(13.2106764271455,2.98323628635612,331.089822980699));
#67909=CARTESIAN_POINT('Ctrl Pts',(13.2029244536213,2.87431864047283,331.00672518952));
#67910=CARTESIAN_POINT('Ctrl Pts',(13.195172480097,2.7618416308738,330.928117057797));
#67911=CARTESIAN_POINT('Ctrl Pts',(13.1874205065728,2.64621463780284,330.854311739508));
#67912=CARTESIAN_POINT('Ctrl Pts',(13.1796718160139,2.53063661283239,330.780537677816));
#67913=CARTESIAN_POINT('Ctrl Pts',(13.1719231254551,2.41191158645138,330.711562593956));
#67914=CARTESIAN_POINT('Ctrl Pts',(13.1641744348963,2.29047888911821,330.647657007886));
#67915=CARTESIAN_POINT('Ctrl Pts',(13.1564273565173,2.1690714568721,330.583764717907));
#67916=CARTESIAN_POINT('Ctrl Pts',(13.1486802781382,2.04495781990597,330.524940009662));
#67917=CARTESIAN_POINT('Ctrl Pts',(13.1409331997592,1.91860259001596,330.471407816541));
#67918=CARTESIAN_POINT('Ctrl Pts',(13.1331860564521,1.79224630114725,330.417875174769));
#67919=CARTESIAN_POINT('Ctrl Pts',(13.1254389131451,1.66364874178968,330.369635289073));
#67920=CARTESIAN_POINT('Ctrl Pts',(13.1176917698381,1.53329484306708,330.326865079337));
#67921=CARTESIAN_POINT('Ctrl Pts',(13.1099428848088,1.40291163802091,330.284085253949));
#67922=CARTESIAN_POINT('Ctrl Pts',(13.1021939997795,1.27077167919907,330.246777673318));
#67923=CARTESIAN_POINT('Ctrl Pts',(13.0944451147502,1.13737502039215,330.21506937088));
#67924=CARTESIAN_POINT('Ctrl Pts',(13.0866880049744,1.0038367729939,330.183327412923));
#67925=CARTESIAN_POINT('Ctrl Pts',(13.0789308951985,0.869039541950893,330.157196695657));
#67926=CARTESIAN_POINT('Ctrl Pts',(13.0711737854226,0.733494085379904,330.136753194705));
#67927=CARTESIAN_POINT('Ctrl Pts',(13.0634125304953,0.597876197650747,330.116298769399));
#67928=CARTESIAN_POINT('Ctrl Pts',(13.0556512755679,0.461509676107818,330.101537658065));
#67929=CARTESIAN_POINT('Ctrl Pts',(13.0478900206406,0.32490937271186,330.092493814367));
#67930=CARTESIAN_POINT('Ctrl Pts',(13.0401163502348,0.188090553348807,330.083435503467));
#67931=CARTESIAN_POINT('Ctrl Pts',(13.032342679829,0.0510375957853707,330.080112745629));
#67932=CARTESIAN_POINT('Ctrl Pts',(13.0245690094232,-0.0857347815890412,
330.082497319805));
#67933=CARTESIAN_POINT('Ctrl Pts',(13.0171572052593,-0.216140371641192,
330.084770891475));
#67934=CARTESIAN_POINT('Ctrl Pts',(13.0097454010953,-0.346290628336729,
330.092232383816));
#67935=CARTESIAN_POINT('Ctrl Pts',(13.0023335969313,-0.475746490519923,
330.104813758471));
#67936=CARTESIAN_POINT('Ctrl Pts',(12.9945585181539,-0.611547370360238,
330.118011783797));
#67937=CARTESIAN_POINT('Ctrl Pts',(12.9867834393765,-0.747013221750016,
330.136885971101));
#67938=CARTESIAN_POINT('Ctrl Pts',(12.9790083605991,-0.881631557619445,
330.161414580778));
#67939=CARTESIAN_POINT('Ctrl Pts',(12.9712428495511,-1.01608423705616,330.185913006439));
#67940=CARTESIAN_POINT('Ctrl Pts',(12.9634773385032,-1.14969109522095,330.216051940399));
#67941=CARTESIAN_POINT('Ctrl Pts',(12.9557118274552,-1.28194343454362,330.251757789125));
#67942=CARTESIAN_POINT('Ctrl Pts',(12.9479540159341,-1.4140646452867,330.287428235399));
#67943=CARTESIAN_POINT('Ctrl Pts',(12.9401962044128,-1.54483363492008,330.328654510873));
#67944=CARTESIAN_POINT('Ctrl Pts',(12.9324383928917,-1.6737509425495,330.375311811072));
#67945=CARTESIAN_POINT('Ctrl Pts',(12.9246864193697,-1.80257123581654,330.421934000172));
#67946=CARTESIAN_POINT('Ctrl Pts',(12.9169344458478,-1.92954225460882,330.473978946502));
#67947=CARTESIAN_POINT('Ctrl Pts',(12.9091824723258,-2.05417912192438,330.531271859069));
#67948=CARTESIAN_POINT('Ctrl Pts',(12.9014337817692,-2.17876320545364,330.588540508053));
#67949=CARTESIAN_POINT('Ctrl Pts',(12.8936850912126,-2.30101474918216,330.65105253993));
#67950=CARTESIAN_POINT('Ctrl Pts',(12.8859364006559,-2.42046852018654,330.718584906215));
#67951=CARTESIAN_POINT('Ctrl Pts',(12.8781893222791,-2.539897437836,330.786103221828));
#67952=CARTESIAN_POINT('Ctrl Pts',(12.8704422439023,-2.65652940055067,330.858639601976));
#67953=CARTESIAN_POINT('Ctrl Pts',(12.8626951655255,-2.76992382894213,330.935925069052));
#67954=CARTESIAN_POINT('Ctrl Pts',(12.8549480222207,-2.88331920768811,331.013211183855));
#67955=CARTESIAN_POINT('Ctrl Pts',(12.8472008789158,-2.99347667500141,331.095246244836));
#67956=CARTESIAN_POINT('Ctrl Pts',(12.839453735611,-3.09998503112164,331.181718204569));
#67957=CARTESIAN_POINT('Ctrl Pts',(12.8317048505839,-3.20651733258199,331.268209605034));
#67958=CARTESIAN_POINT('Ctrl Pts',(12.8239559655567,-3.30939858695373,331.359139642861));
#67959=CARTESIAN_POINT('Ctrl Pts',(12.8162070805296,-3.40825136131104,331.454156557232));
#67960=CARTESIAN_POINT('Ctrl Pts',(12.8084499707558,-3.50720905902468,331.549274323537));
#67961=CARTESIAN_POINT('Ctrl Pts',(12.800692860982,-3.6021294530234,331.648487360358));
#67962=CARTESIAN_POINT('Ctrl Pts',(12.7929357512082,-3.69267225326139,331.751407275066));
#67963=CARTESIAN_POINT('Ctrl Pts',(12.785174496283,-3.78326343667678,331.854382186886));
#67964=CARTESIAN_POINT('Ctrl Pts',(12.7774132413578,-3.86947211962819,331.961067619721));
#67965=CARTESIAN_POINT('Ctrl Pts',(12.7696519864326,-3.95099954302915,332.071043586278));
#67966=CARTESIAN_POINT('Ctrl Pts',(12.7618783160288,-4.03265738373829,332.181195478541));
#67967=CARTESIAN_POINT('Ctrl Pts',(12.7541046456251,-4.10961878113251,332.294648099478));
#67968=CARTESIAN_POINT('Ctrl Pts',(12.7463309752213,-4.18162892323844,332.410953339386));
#67969=CARTESIAN_POINT('Ctrl Pts',(12.7389191710333,-4.25028697601363,332.521844542571));
#67970=CARTESIAN_POINT('Ctrl Pts',(12.7315073668454,-4.31444422005825,332.635328512064));
#67971=CARTESIAN_POINT('Ctrl Pts',(12.7240955626574,-4.37392026909127,332.75099921251));
#67972=CARTESIAN_POINT('Ctrl Pts',(12.7158245986272,-4.44029064932982,332.880078203058));
#67973=CARTESIAN_POINT('Ctrl Pts',(12.707553634597,-4.50102026115738,333.012246799271));
#67974=CARTESIAN_POINT('Ctrl Pts',(12.6992826705668,-4.55582953802183,333.147002352136));
#67975=CARTESIAN_POINT('Ctrl Pts',(12.6910273949352,-4.61053485242457,333.281502300115));
#67976=CARTESIAN_POINT('Ctrl Pts',(12.6827721193036,-4.65934209626467,333.418579133346));
#67977=CARTESIAN_POINT('Ctrl Pts',(12.674516843672,-4.70201793527007,333.557706548965));
#67978=CARTESIAN_POINT('Ctrl Pts',(12.6662830903639,-4.74458251412426,333.696471245592));
#67979=CARTESIAN_POINT('Ctrl Pts',(12.6580493370559,-4.78104747464785,333.837275562377));
#67980=CARTESIAN_POINT('Ctrl Pts',(12.6498155837478,-4.81122811232962,333.979575032827));
#67981=CARTESIAN_POINT('Ctrl Pts',(12.6415950492509,-4.84136029675637,334.12164604977));
#67982=CARTESIAN_POINT('Ctrl Pts',(12.6333745147539,-4.86522819715475,334.265207130258));
#67983=CARTESIAN_POINT('Ctrl Pts',(12.625153980257,-4.88269671584385,334.409698514666));
#67984=CARTESIAN_POINT('Ctrl Pts',(12.6169511416217,-4.90012763107903,334.553878860959));
#67985=CARTESIAN_POINT('Ctrl Pts',(12.6087483029864,-4.91118659541477,334.698985205665));
#67986=CARTESIAN_POINT('Ctrl Pts',(12.6005454643512,-4.91578952414677,334.844448025442));
#67987=CARTESIAN_POINT('Ctrl Pts',(12.5976361017467,-4.91742207957295,334.896040420103));
#67988=CARTESIAN_POINT('Ctrl Pts',(12.5947267391421,-4.91824295710074,334.947677557148));
#67989=CARTESIAN_POINT('Ctrl Pts',(12.5918173765376,-4.91824995487103,334.99933373343));
#67990=CARTESIAN_POINT('',(10.8418173764557,-4.91824791560711,335.004528037799));
#67991=CARTESIAN_POINT('Ctrl Pts',(12.5918173765088,-4.9182499548711,334.999333733942));
#67992=CARTESIAN_POINT('Ctrl Pts',(12.5837801713581,-4.91826928641542,335.142035535853));
#67993=CARTESIAN_POINT('Ctrl Pts',(12.5757429662075,-4.91207359840828,335.284645054202));
#67994=CARTESIAN_POINT('Ctrl Pts',(12.5677057610568,-4.89971296326426,335.426609821875));
#67995=CARTESIAN_POINT('Ctrl Pts',(12.5596606460499,-4.88734016333841,335.568714304894));
#67996=CARTESIAN_POINT('Ctrl Pts',(12.551615531043,-4.8687903455266,335.710172426349));
#67997=CARTESIAN_POINT('Ctrl Pts',(12.5435704160361,-4.84416512844621,335.850439457484));
#67998=CARTESIAN_POINT('Ctrl Pts',(12.5354276753984,-4.81924108998801,335.992408596965));
#67999=CARTESIAN_POINT('Ctrl Pts',(12.5272849347606,-4.78809332468382,336.13315719114));
#68000=CARTESIAN_POINT('Ctrl Pts',(12.5191421941229,-4.75087933018811,336.272135469394));
#68001=CARTESIAN_POINT('Ctrl Pts',(12.5110723034859,-4.71399827513448,336.4098703619));
#68002=CARTESIAN_POINT('Ctrl Pts',(12.5030024128489,-4.67115927453661,336.545866181394));
#68003=CARTESIAN_POINT('Ctrl Pts',(12.4949325222119,-4.62256446220816,336.679607351505));
#68004=CARTESIAN_POINT('Ctrl Pts',(12.4867533565739,-4.57331162384106,336.815159520942));
#68005=CARTESIAN_POINT('Ctrl Pts',(12.4785741909358,-4.51814612085063,336.94839519872));
#68006=CARTESIAN_POINT('Ctrl Pts',(12.4703950252977,-4.45732674295449,337.078802869212));
#68007=CARTESIAN_POINT('Ctrl Pts',(12.4622158596597,-4.39650736505842,337.209210539704));
#68008=CARTESIAN_POINT('Ctrl Pts',(12.4540366940216,-4.33003433733722,337.336789909527));
#68009=CARTESIAN_POINT('Ctrl Pts',(12.4458575283836,-4.25821197560238,337.461059494067));
#68010=CARTESIAN_POINT('Ctrl Pts',(12.438082449597,-4.18993795526356,337.579189613119));
#68011=CARTESIAN_POINT('Ctrl Pts',(12.4303073708104,-4.1166366253402,337.694663189806));
#68012=CARTESIAN_POINT('Ctrl Pts',(12.4225322920238,-4.03854009400104,337.807022794999));
#68013=CARTESIAN_POINT('Ctrl Pts',(12.4147667809667,-3.96053966541536,337.919244134546));
#68014=CARTESIAN_POINT('Ctrl Pts',(12.4070012699095,-3.87775599726861,338.02835880917));
#68015=CARTESIAN_POINT('Ctrl Pts',(12.3992357588523,-3.79046682216597,338.133934321673));
#68016=CARTESIAN_POINT('Ctrl Pts',(12.3914779473219,-3.70326419453443,338.239405155748));
#68017=CARTESIAN_POINT('Ctrl Pts',(12.3837201357915,-3.61156519743657,338.341343511684));
#68018=CARTESIAN_POINT('Ctrl Pts',(12.3759623242612,-3.51569034595541,338.439346515525));
#68019=CARTESIAN_POINT('Ctrl Pts',(12.36821035073,-3.41988764334016,338.537275768998));
#68020=CARTESIAN_POINT('Ctrl Pts',(12.3604583771988,-3.3199156134992,338.63127528677));
#68021=CARTESIAN_POINT('Ctrl Pts',(12.3527064036676,-3.21613422425481,338.720976177574));
#68022=CARTESIAN_POINT('Ctrl Pts',(12.3449577131019,-3.11239678649104,338.810639079998));
#68023=CARTESIAN_POINT('Ctrl Pts',(12.3372090225361,-3.00485349310262,338.896006721174));
#68024=CARTESIAN_POINT('Ctrl Pts',(12.3294603319704,-2.89390009456913,338.976748081681));
#68025=CARTESIAN_POINT('Ctrl Pts',(12.3217132535844,-2.78296978081719,339.057472643273));
#68026=CARTESIAN_POINT('Ctrl Pts',(12.3139661751985,-2.66863108901826,339.133572608903));
#68027=CARTESIAN_POINT('Ctrl Pts',(12.3062190968126,-2.55131135776195,339.204758425671));
#68028=CARTESIAN_POINT('Ctrl Pts',(12.2984719534987,-2.43399064325393,339.275944839045));
#68029=CARTESIAN_POINT('Ctrl Pts',(12.2907248101848,-2.31368917362621,339.342216818646));
#68030=CARTESIAN_POINT('Ctrl Pts',(12.2829776668709,-2.19086131519886,339.403329394908));
#68031=CARTESIAN_POINT('Ctrl Pts',(12.2752287818348,-2.06800584246158,339.464455710576));
#68032=CARTESIAN_POINT('Ctrl Pts',(12.2674798967986,-1.94262320057929,339.520420140665));
#68033=CARTESIAN_POINT('Ctrl Pts',(12.2597310117625,-1.81518991116986,339.571024901364));
#68034=CARTESIAN_POINT('Ctrl Pts',(12.2519739019798,-1.68762136275247,339.621683374478));
#68035=CARTESIAN_POINT('Ctrl Pts',(12.2442167921971,-1.55799818274094,339.666970669785));
#68036=CARTESIAN_POINT('Ctrl Pts',(12.2364596824145,-1.42681484468761,339.706737985216));
#68037=CARTESIAN_POINT('Ctrl Pts',(12.2286984274804,-1.29556140645355,339.746526551029));
#68038=CARTESIAN_POINT('Ctrl Pts',(12.2209371725463,-1.16274652724934,339.780789161833));
#68039=CARTESIAN_POINT('Ctrl Pts',(12.2131759176123,-1.02887623007913,339.809427904198));
#68040=CARTESIAN_POINT('Ctrl Pts',(12.2054022471999,-0.894791784064626,
339.838112459217));
#68041=CARTESIAN_POINT('Ctrl Pts',(12.1976285767875,-0.759648931827385,
339.86115510268));
#68042=CARTESIAN_POINT('Ctrl Pts',(12.1898549063751,-0.623961084570843,
339.878509570293));
#68043=CARTESIAN_POINT('Ctrl Pts',(12.1824431022865,-0.494589540922598,
339.895056183049));
#68044=CARTESIAN_POINT('Ctrl Pts',(12.1750312981979,-0.36472288615217,339.906432246523));
#68045=CARTESIAN_POINT('Ctrl Pts',(12.1676194941094,-0.234805403461494,
339.912641803043));
#68046=CARTESIAN_POINT('Ctrl Pts',(12.1598444153398,-0.0985202764682728,
339.919155708496));
#68047=CARTESIAN_POINT('Ctrl Pts',(12.1520693365704,0.0382514730609481,
339.920004434583));
#68048=CARTESIAN_POINT('Ctrl Pts',(12.1442942578008,0.17499957616798,339.915135624867));
#68049=CARTESIAN_POINT('Ctrl Pts',(12.1365287467607,0.311579402028877,339.910272806532));
#68050=CARTESIAN_POINT('Ctrl Pts',(12.1287632357205,0.448135252472564,339.899706465376));
#68051=CARTESIAN_POINT('Ctrl Pts',(12.1209977246804,0.584153134330435,339.883436103621));
#68052=CARTESIAN_POINT('Ctrl Pts',(12.113239913167,0.720036154063117,339.867181873977));
#68053=CARTESIAN_POINT('Ctrl Pts',(12.1054821016535,0.855381881093607,339.845234924731));
#68054=CARTESIAN_POINT('Ctrl Pts',(12.0977242901401,0.989678081016159,339.817646765637));
#68055=CARTESIAN_POINT('Ctrl Pts',(12.0899723166259,1.12387321878993,339.790079367508));
#68056=CARTESIAN_POINT('Ctrl Pts',(12.0822203431118,1.25702002018162,339.756879287711));
#68057=CARTESIAN_POINT('Ctrl Pts',(12.0744683695976,1.3886134774134,339.718149602635));
#68058=CARTESIAN_POINT('Ctrl Pts',(12.0667196790486,1.52015120473965,339.679436319603));
#68059=CARTESIAN_POINT('Ctrl Pts',(12.0589709884997,1.65013652211661,339.635198199079));
#68060=CARTESIAN_POINT('Ctrl Pts',(12.0512222979507,1.77807690495904,339.58558890248));
#68061=CARTESIAN_POINT('Ctrl Pts',(12.0434752195815,1.90599066873726,339.53598992751));
#68062=CARTESIAN_POINT('Ctrl Pts',(12.0357281412122,2.03185998005482,339.481022140509));
#68063=CARTESIAN_POINT('Ctrl Pts',(12.027981062843,2.15521009027124,339.420888205926));
#68064=CARTESIAN_POINT('Ctrl Pts',(12.0202339195457,2.27856123428174,339.360753767362));
#68065=CARTESIAN_POINT('Ctrl Pts',(12.0124867762485,2.39939278373208,339.295453266139));
#68066=CARTESIAN_POINT('Ctrl Pts',(12.0047396329512,2.517252854803,339.225236221501));
#68067=CARTESIAN_POINT('Ctrl Pts',(11.9969907479316,2.63513942332097,339.155003390581));
#68068=CARTESIAN_POINT('Ctrl Pts',(11.9892418629119,2.75005284837986,339.079852016752));
#68069=CARTESIAN_POINT('Ctrl Pts',(11.9814929778923,2.8615689361648,339.000075785042));
#68070=CARTESIAN_POINT('Ctrl Pts',(11.9737358681259,2.97320338828035,338.920214878012));
#68071=CARTESIAN_POINT('Ctrl Pts',(11.9659787583594,3.08143298145544,338.835719534948));
#68072=CARTESIAN_POINT('Ctrl Pts',(11.958221648593,3.18586499684499,338.74692504387));
#68073=CARTESIAN_POINT('Ctrl Pts',(11.950460393675,3.29035281736574,338.658083103853));
#68074=CARTESIAN_POINT('Ctrl Pts',(11.942699138757,3.39103872975003,338.564937703493));
#68075=CARTESIAN_POINT('Ctrl Pts',(11.934937883839,3.48756655842495,338.467861381753));
#68076=CARTESIAN_POINT('Ctrl Pts',(11.9271642134423,3.58424880017019,338.370629769533));
#68077=CARTESIAN_POINT('Ctrl Pts',(11.9193905430457,3.67675940248055,338.269454958878));
#68078=CARTESIAN_POINT('Ctrl Pts',(11.911616872649,3.7647816244639,338.164743651956));
#68079=CARTESIAN_POINT('Ctrl Pts',(11.9042050683778,3.84870639198813,338.064906680195));
#68080=CARTESIAN_POINT('Ctrl Pts',(11.8967932641067,3.92855106715021,337.961855277865));
#68081=CARTESIAN_POINT('Ctrl Pts',(11.8893814598356,4.00407862208117,337.855965239756));
#68082=CARTESIAN_POINT('Ctrl Pts',(11.881606381068,4.08330800634825,337.744885217013));
#68083=CARTESIAN_POINT('Ctrl Pts',(11.8738313023004,4.15803675980889,337.630330229376));
#68084=CARTESIAN_POINT('Ctrl Pts',(11.8660562235328,4.2279447190047,337.512701039826));
#68085=CARTESIAN_POINT('Ctrl Pts',(11.8582907124948,4.29776665200489,337.395216600483));
#68086=CARTESIAN_POINT('Ctrl Pts',(11.8505252014567,4.36277939651893,337.274665819115));
#68087=CARTESIAN_POINT('Ctrl Pts',(11.8427596904187,4.42270438275697,337.151480654164));
#68088=CARTESIAN_POINT('Ctrl Pts',(11.8350018789076,4.4825699531959,337.028417627665));
#68089=CARTESIAN_POINT('Ctrl Pts',(11.8272440673965,4.5373576343673,336.902725764835));
#68090=CARTESIAN_POINT('Ctrl Pts',(11.8194862558854,4.58683354249418,336.7748636894));
#68091=CARTESIAN_POINT('Ctrl Pts',(11.8117342823735,4.63627221843062,336.647097834233));
#68092=CARTESIAN_POINT('Ctrl Pts',(11.8039823088617,4.68040693722041,336.517165380239));
#68093=CARTESIAN_POINT('Ctrl Pts',(11.7962303353498,4.71905108931182,336.385546779782));
#68094=CARTESIAN_POINT('Ctrl Pts',(11.7884816448034,4.75767887558134,336.253983919883));
#68095=CARTESIAN_POINT('Ctrl Pts',(11.7807329542571,4.79082061004134,336.120736708045));
#68096=CARTESIAN_POINT('Ctrl Pts',(11.7729842637107,4.81833897654101,335.98630247371));
#68097=CARTESIAN_POINT('Ctrl Pts',(11.7652371853442,4.84585161761446,335.851896209541));
#68098=CARTESIAN_POINT('Ctrl Pts',(11.7574901069777,4.86774313958145,335.716303796809));
#68099=CARTESIAN_POINT('Ctrl Pts',(11.7497430286112,4.88392705356856,335.580034135134));
#68100=CARTESIAN_POINT('Ctrl Pts',(11.7419958853168,4.90011110319238,335.44376333139));
#68101=CARTESIAN_POINT('Ctrl Pts',(11.7342487420223,4.9105874033276,335.306815655528));
#68102=CARTESIAN_POINT('Ctrl Pts',(11.7265015987279,4.91532123976476,335.169706135474));
#68103=CARTESIAN_POINT('Ctrl Pts',(11.7187527137111,4.92005614046884,335.032565790288));
#68104=CARTESIAN_POINT('Ctrl Pts',(11.7110038286944,4.91904599498924,334.895263919071));
#68105=CARTESIAN_POINT('Ctrl Pts',(11.7032549436777,4.91230821371474,334.758316165268));
#68106=CARTESIAN_POINT('Ctrl Pts',(11.6954978339144,4.90556328088958,334.621223053705));
#68107=CARTESIAN_POINT('Ctrl Pts',(11.6877407241511,4.89307858739198,334.484485201398));
#68108=CARTESIAN_POINT('Ctrl Pts',(11.6799836143877,4.87492356136952,334.34861429759));
#68109=CARTESIAN_POINT('Ctrl Pts',(11.672222359473,4.85675883388164,334.212670788715));
#68110=CARTESIAN_POINT('Ctrl Pts',(11.6644611045581,4.83291780413792,334.077595536174));
#68111=CARTESIAN_POINT('Ctrl Pts',(11.6566998496434,4.80352100106055,333.943889657815));
#68112=CARTESIAN_POINT('Ctrl Pts',(11.64892617925,4.77407717267822,333.809969893623));
#68113=CARTESIAN_POINT('Ctrl Pts',(11.6411525088566,4.73905991114379,333.677424259092));
#68114=CARTESIAN_POINT('Ctrl Pts',(11.6333788384633,4.69863981431569,333.546739198276));
#68115=CARTESIAN_POINT('Ctrl Pts',(11.6259670341627,4.66010128202142,333.422137556225));
#68116=CARTESIAN_POINT('Ctrl Pts',(11.6185552298622,4.61665169435156,333.299227438073));
#68117=CARTESIAN_POINT('Ctrl Pts',(11.6111434255616,4.56847879578283,333.17841152974));
#68118=CARTESIAN_POINT('Ctrl Pts',(11.6033683467292,4.51794480044675,333.05167407508));
#68119=CARTESIAN_POINT('Ctrl Pts',(11.5955932678969,4.46205308333984,332.92684079404));
#68120=CARTESIAN_POINT('Ctrl Pts',(11.5878181890645,4.40096739579065,332.804397794753));
#68121=CARTESIAN_POINT('Ctrl Pts',(11.5800526779614,4.33995687806763,332.682105469368));
#68122=CARTESIAN_POINT('Ctrl Pts',(11.5722871668584,4.27376528000271,332.562197919625));
#68123=CARTESIAN_POINT('Ctrl Pts',(11.5645216557553,4.20260509457612,332.445143158308));
#68124=CARTESIAN_POINT('Ctrl Pts',(11.556763844179,4.13151546467916,332.328204457124));
#68125=CARTESIAN_POINT('Ctrl Pts',(11.5490060326026,4.05546725291025,332.214113247243));
#68126=CARTESIAN_POINT('Ctrl Pts',(11.5412482210263,3.97471955781791,332.103314394139));
#68127=CARTESIAN_POINT('Ctrl Pts',(11.5334962474491,3.89403262792669,331.992598920686));
#68128=CARTESIAN_POINT('Ctrl Pts',(11.525744273872,3.80865348324775,331.885171187078));
#68129=CARTESIAN_POINT('Ctrl Pts',(11.5179923002948,3.71888516129336,331.781448117614));
#68130=CARTESIAN_POINT('Ctrl Pts',(11.5102436096833,3.62915485627842,331.677768974933));
#68131=CARTESIAN_POINT('Ctrl Pts',(11.5024949190717,3.53503932630827,331.577791670851));
#68132=CARTESIAN_POINT('Ctrl Pts',(11.4947462284601,3.43688247667781,331.481900810949));
#68133=CARTESIAN_POINT('Ctrl Pts',(11.4869991500285,3.33874604940094,331.386029901941));
#68134=CARTESIAN_POINT('Ctrl Pts',(11.4792520715969,3.23657025435759,331.294244018941));
#68135=CARTESIAN_POINT('Ctrl Pts',(11.4715049931652,3.13073623201036,331.206891287074));
#68136=CARTESIAN_POINT('Ctrl Pts',(11.4637578498057,3.02490132267454,331.119537823109));
#68137=CARTESIAN_POINT('Ctrl Pts',(11.4560107064462,2.91540842633691,331.036617833197));
#68138=CARTESIAN_POINT('Ctrl Pts',(11.4482635630868,2.80267185512178,330.958439220424));
#68139=CARTESIAN_POINT('Ctrl Pts',(11.4405146780053,2.68990993833552,330.880243031441));
#68140=CARTESIAN_POINT('Ctrl Pts',(11.4327657929238,2.57390321668924,330.806790563438));
#68141=CARTESIAN_POINT('Ctrl Pts',(11.4250169078423,2.45509472752491,330.738346219907));
#68142=CARTESIAN_POINT('Ctrl Pts',(11.4172597980147,2.33616013381324,330.669829228849));
#68143=CARTESIAN_POINT('Ctrl Pts',(11.4095026881873,2.21441817131636,330.606331176248));
#68144=CARTESIAN_POINT('Ctrl Pts',(11.4017455783597,2.09033670199461,330.548070582905));
#68145=CARTESIAN_POINT('Ctrl Pts',(11.3939843233811,1.9661889275081,330.489778856966));
#68146=CARTESIAN_POINT('Ctrl Pts',(11.3862230684024,1.83969951541976,330.436730318105));
#68147=CARTESIAN_POINT('Ctrl Pts',(11.3784618134237,1.71135509154057,330.389094794603));
#68148=CARTESIAN_POINT('Ctrl Pts',(11.3706881429675,1.58280535842797,330.341383069794));
#68149=CARTESIAN_POINT('Ctrl Pts',(11.3629144725113,1.45239505576822,330.299101784325));
#68150=CARTESIAN_POINT('Ctrl Pts',(11.3551408020551,1.32062556504041,330.26237072161));
#68151=CARTESIAN_POINT('Ctrl Pts',(11.347728998466,1.19498998660669,330.227349501711));
#68152=CARTESIAN_POINT('Ctrl Pts',(11.3403171948769,1.06811919309805,330.197373472726));
#68153=CARTESIAN_POINT('Ctrl Pts',(11.3329053912877,0.940453410873421,330.172502672763));
#68154=CARTESIAN_POINT('Ctrl Pts',(11.3251303125808,0.8065303389734,330.146412878979));
#68155=CARTESIAN_POINT('Ctrl Pts',(11.3173552338738,0.671309156618477,330.125858965163));
#68156=CARTESIAN_POINT('Ctrl Pts',(11.3095801551669,0.535287257732207,330.110966290338));
#68157=CARTESIAN_POINT('Ctrl Pts',(11.3018146441893,0.399432742451233,330.096091941898));
#68158=CARTESIAN_POINT('Ctrl Pts',(11.2940491332117,0.262779856006339,330.086865013215));
#68159=CARTESIAN_POINT('Ctrl Pts',(11.286283622234,0.125837152462086,330.083360082988));
#68160=CARTESIAN_POINT('Ctrl Pts',(11.278525810783,-0.0109697719956586,
330.079858627908));
#68161=CARTESIAN_POINT('Ctrl Pts',(11.2707679993319,-0.148065553471827,
330.082067890877));
#68162=CARTESIAN_POINT('Ctrl Pts',(11.2630101878808,-0.284935882019815,
330.090010732635));
#68163=CARTESIAN_POINT('Ctrl Pts',(11.2552582144286,-0.421703211309805,
330.097947597154));
#68164=CARTESIAN_POINT('Ctrl Pts',(11.2475062409764,-0.558245036725915,
330.11160942971));
#68165=CARTESIAN_POINT('Ctrl Pts',(11.2397542675242,-0.694046766757465,
330.13096702126));
#68166=CARTESIAN_POINT('Ctrl Pts',(11.2320055770366,-0.829790984687955,
330.150316414861));
#68167=CARTESIAN_POINT('Ctrl Pts',(11.2242568865492,-0.964795344468126,
330.175356714802));
#68168=CARTESIAN_POINT('Ctrl Pts',(11.2165081960616,-1.0985503161835,330.206006855938));
#68169=CARTESIAN_POINT('Ctrl Pts',(11.2087611177534,-1.23227745906762,330.236650620058));
#68170=CARTESIAN_POINT('Ctrl Pts',(11.2010140394452,-1.36475535017717,330.272901816529));
#68171=CARTESIAN_POINT('Ctrl Pts',(11.193266961137,-1.49548498670334,330.314628326691));
#68172=CARTESIAN_POINT('Ctrl Pts',(11.1855198179003,-1.62621571887834,330.356355186565));
#68173=CARTESIAN_POINT('Ctrl Pts',(11.1777726746637,-1.75519779487862,330.403557332806));
#68174=CARTESIAN_POINT('Ctrl Pts',(11.170025531427,-1.88194808438028,330.456052985542));
#68175=CARTESIAN_POINT('Ctrl Pts',(11.1622766464675,-2.00872687004673,330.50856044042));
#68176=CARTESIAN_POINT('Ctrl Pts',(11.154527761508,-2.13327250972557,330.566363620406));
#68177=CARTESIAN_POINT('Ctrl Pts',(11.1467788765485,-2.25512290796421,330.629233049856));
#68178=CARTESIAN_POINT('Ctrl Pts',(11.1390217668411,-2.37710263949621,330.692169209578));
#68179=CARTESIAN_POINT('Ctrl Pts',(11.1312646571336,-2.49638106704423,330.760182181059));
#68180=CARTESIAN_POINT('Ctrl Pts',(11.1235075474261,-2.61252124486372,330.832996783342));
#68181=CARTESIAN_POINT('Ctrl Pts',(11.1157462925667,-2.72872348429026,330.905850295427));
#68182=CARTESIAN_POINT('Ctrl Pts',(11.1079850377072,-2.84178381042839,330.983510329784));
#68183=CARTESIAN_POINT('Ctrl Pts',(11.1002237828478,-2.95129606991621,331.065659576219));
#68184=CARTESIAN_POINT('Ctrl Pts',(11.0924501125081,-3.06098351335428,331.147940234695));
#68185=CARTESIAN_POINT('Ctrl Pts',(11.0846764421684,-3.16711124556448,331.234724208004));
#68186=CARTESIAN_POINT('Ctrl Pts',(11.0769027718288,-3.26930721184414,331.325654695448));
#68187=CARTESIAN_POINT('Ctrl Pts',(11.0694909668904,-3.36674594212936,331.412352356454));
#68188=CARTESIAN_POINT('Ctrl Pts',(11.0620791619521,-3.46061050821,331.50281897985));
#68189=CARTESIAN_POINT('Ctrl Pts',(11.0546673570138,-3.55061219086199,331.596716859766));
#68190=CARTESIAN_POINT('Ctrl Pts',(11.0469901530241,-3.64383661903929,331.693976998736));
#68191=CARTESIAN_POINT('Ctrl Pts',(11.0393129490344,-3.73322755412441,331.795243674666));
#68192=CARTESIAN_POINT('Ctrl Pts',(11.0316357450447,-3.81841425428008,331.900178126858));
#68193=CARTESIAN_POINT('Ctrl Pts',(11.0237266463557,-3.9061740714509,332.00828218914));
#68194=CARTESIAN_POINT('Ctrl Pts',(11.0158175476667,-3.98947129927634,332.120278873941));
#68195=CARTESIAN_POINT('Ctrl Pts',(11.0079084489777,-4.06793948211894,332.235754816895));
#68196=CARTESIAN_POINT('Ctrl Pts',(11.0002501000046,-4.14391991315414,332.347569715648));
#68197=CARTESIAN_POINT('Ctrl Pts',(10.9925917510315,-4.21537257413328,332.46264626105));
#68198=CARTESIAN_POINT('Ctrl Pts',(10.9849334020585,-4.2820045498982,332.580574428268));
#68199=CARTESIAN_POINT('Ctrl Pts',(10.9772800314538,-4.34859321103718,332.698425935378));
#68200=CARTESIAN_POINT('Ctrl Pts',(10.9696266608492,-4.41036722147423,332.819125029996));
#68201=CARTESIAN_POINT('Ctrl Pts',(10.9619732902445,-4.46707714790624,332.942233050816));
#68202=CARTESIAN_POINT('Ctrl Pts',(10.9543231381244,-4.5237632260189,333.065289300817));
#68203=CARTESIAN_POINT('Ctrl Pts',(10.9466729860044,-4.57538928856949,333.190752097796));
#68204=CARTESIAN_POINT('Ctrl Pts',(10.9390228338843,-4.62175226534308,333.318159026455));
#68205=CARTESIAN_POINT('Ctrl Pts',(10.9313741432867,-4.66810638470703,333.445541614671));
#68206=CARTESIAN_POINT('Ctrl Pts',(10.923725452689,-4.7091992830285,333.574867217875));
#68207=CARTESIAN_POINT('Ctrl Pts',(10.9160767620914,-4.7448765710052,333.70565484185));
#68208=CARTESIAN_POINT('Ctrl Pts',(10.9084255677315,-4.78056553777153,333.836485278528));
#68209=CARTESIAN_POINT('Ctrl Pts',(10.9007743733717,-4.81083524547869,333.968778304757));
#68210=CARTESIAN_POINT('Ctrl Pts',(10.8931231790118,-4.83558162769242,334.10203931911));
#68211=CARTESIAN_POINT('Ctrl Pts',(10.8854704134292,-4.86033309173711,334.235327699482));
#68212=CARTESIAN_POINT('Ctrl Pts',(10.8778176478466,-4.8795589094284,334.369584067083));
#68213=CARTESIAN_POINT('Ctrl Pts',(10.870164882264,-4.8932065976908,334.504306289312));
#68214=CARTESIAN_POINT('Ctrl Pts',(10.8625062805538,-4.90686469390964,334.639131252972));
#68215=CARTESIAN_POINT('Ctrl Pts',(10.8548476788436,-4.91493614280631,334.774422380051));
#68216=CARTESIAN_POINT('Ctrl Pts',(10.8471890771334,-4.9174205114799,334.909675165227));
#68217=CARTESIAN_POINT('Ctrl Pts',(10.8453985102585,-4.91800135226785,334.941297015538));
#68218=CARTESIAN_POINT('Ctrl Pts',(10.8436079433837,-4.91827701884567,334.972916779595));
#68219=CARTESIAN_POINT('Ctrl Pts',(10.8418173765088,-4.91824791560797,335.004528036861));
#68220=CARTESIAN_POINT('',(9.09181737647954,-4.91824973135284,334.998374408491));
#68221=CARTESIAN_POINT('Ctrl Pts',(10.8418173764556,-4.91824791560711,335.004528037799));
#68222=CARTESIAN_POINT('Ctrl Pts',(10.8316241091295,-4.91808223782791,335.184483335951));
#68223=CARTESIAN_POINT('Ctrl Pts',(10.8214308418033,-4.90803654552355,335.364000285683));
#68224=CARTESIAN_POINT('Ctrl Pts',(10.8112375744772,-4.88827494979252,335.542172553465));
#68225=CARTESIAN_POINT('Ctrl Pts',(10.8007669046654,-4.86797555635617,335.725193652185));
#68226=CARTESIAN_POINT('Ctrl Pts',(10.7902962348536,-4.8374241868972,335.906796289323));
#68227=CARTESIAN_POINT('Ctrl Pts',(10.7798255650418,-4.79684630554198,336.086024209449));
#68228=CARTESIAN_POINT('Ctrl Pts',(10.7786934842745,-4.79245905621744,336.105402194332));
#68229=CARTESIAN_POINT('Ctrl Pts',(10.7775614035072,-4.78795464471481,336.124752440221));
#68230=CARTESIAN_POINT('Ctrl Pts',(10.7764293227399,-4.78333338899957,336.144073752947));
#68231=CARTESIAN_POINT('Ctrl Pts',(10.7686542436122,-4.75159481530949,336.276771648393));
#68232=CARTESIAN_POINT('Ctrl Pts',(10.7608791644844,-4.71428000280257,336.408357507293));
#68233=CARTESIAN_POINT('Ctrl Pts',(10.7531040853567,-4.6714809260607,336.538326694805));
#68234=CARTESIAN_POINT('Ctrl Pts',(10.7453385739574,-4.62873451629988,336.668135946982));
#68235=CARTESIAN_POINT('Ctrl Pts',(10.7375730625581,-4.58051739144098,336.796332118426));
#68236=CARTESIAN_POINT('Ctrl Pts',(10.7298075511588,-4.52697236696789,336.922421455147));
#68237=CARTESIAN_POINT('Ctrl Pts',(10.7220497392858,-4.47348043253603,337.048385773939));
#68238=CARTESIAN_POINT('Ctrl Pts',(10.7142919274127,-4.41467126301592,337.172247057642));
#68239=CARTESIAN_POINT('Ctrl Pts',(10.7065341155397,-4.35073712919702,337.293527740213));
#68240=CARTESIAN_POINT('Ctrl Pts',(10.6987821416656,-4.28685110783728,337.414717155232));
#68241=CARTESIAN_POINT('Ctrl Pts',(10.6910301677915,-4.21784798028972,337.533329490164));
#68242=CARTESIAN_POINT('Ctrl Pts',(10.6832781939174,-4.14396752487062,337.648908495082));
#68243=CARTESIAN_POINT('Ctrl Pts',(10.6755295030096,-4.07011835787539,337.764438552211));
#68244=CARTESIAN_POINT('Ctrl Pts',(10.6677808121018,-3.99139618132735,337.876937505686));
#68245=CARTESIAN_POINT('Ctrl Pts',(10.660032121194,-3.90808587293053,337.985975196197));
#68246=CARTESIAN_POINT('Ctrl Pts',(10.6522850424666,-3.82479289794488,338.094990200497));
#68247=CARTESIAN_POINT('Ctrl Pts',(10.6445379637392,-3.73691392703545,338.200545063856));
#68248=CARTESIAN_POINT('Ctrl Pts',(10.6367908850117,-3.64477594247839,338.302240359458));
#68249=CARTESIAN_POINT('Ctrl Pts',(10.6290437413573,-3.55263718572722,338.403936507351));
#68250=CARTESIAN_POINT('Ctrl Pts',(10.6212965977028,-3.45623960657688,338.501772733305));
#68251=CARTESIAN_POINT('Ctrl Pts',(10.6135494540483,-3.35594881010928,338.595384631222));
#68252=CARTESIAN_POINT('Ctrl Pts',(10.6058005686728,-3.2556354661588,338.689017575065));
#68253=CARTESIAN_POINT('Ctrl Pts',(10.5980516832972,-3.15142744887184,338.778424034379));
#68254=CARTESIAN_POINT('Ctrl Pts',(10.5903027979217,-3.04372505854441,338.863278508015));
#68255=CARTESIAN_POINT('Ctrl Pts',(10.5825456878035,-2.93590835184696,338.948223047018));
#68256=CARTESIAN_POINT('Ctrl Pts',(10.5747885776854,-2.82459017062622,339.028605706644));
#68257=CARTESIAN_POINT('Ctrl Pts',(10.5670314675672,-2.71020199402079,339.104142811125));
#68258=CARTESIAN_POINT('Ctrl Pts',(10.5592702122992,-2.59575269205733,339.179720280202));
#68259=CARTESIAN_POINT('Ctrl Pts',(10.5515089570311,-2.47823046058554,339.250446833256));
#68260=CARTESIAN_POINT('Ctrl Pts',(10.543747701763,-2.35809236511287,339.31608427398));
#68261=CARTESIAN_POINT('Ctrl Pts',(10.5359740310227,-2.23776208794456,339.381826713161));
#68262=CARTESIAN_POINT('Ctrl Pts',(10.5282003602823,-2.11480793559586,339.442463599073));
#68263=CARTESIAN_POINT('Ctrl Pts',(10.520426689542,-1.98970878854097,339.497804130829));
#68264=CARTESIAN_POINT('Ctrl Pts',(10.5130148891833,-1.870433103477,339.550568518056));
#68265=CARTESIAN_POINT('Ctrl Pts',(10.5056030888245,-1.74920789841154,339.598518444527));
#68266=CARTESIAN_POINT('Ctrl Pts',(10.4981912884658,-1.62646014828702,339.641531045736));
#68267=CARTESIAN_POINT('Ctrl Pts',(10.4904162102366,-1.49769610804178,339.686651842716));
#68268=CARTESIAN_POINT('Ctrl Pts',(10.4826411320073,-1.36684958044363,339.726481676002));
#68269=CARTESIAN_POINT('Ctrl Pts',(10.4748660537781,-1.23439469630777,339.760824802093));
#68270=CARTESIAN_POINT('Ctrl Pts',(10.4671005432775,-1.10210280633826,339.795125666782));
#68271=CARTESIAN_POINT('Ctrl Pts',(10.459335032777,-0.968206872587985,339.823953161143));
#68272=CARTESIAN_POINT('Ctrl Pts',(10.4515695222765,-0.833199388867935,
339.847160183127));
#68273=CARTESIAN_POINT('Ctrl Pts',(10.4438117113015,-0.698325765448033,
339.870344195283));
#68274=CARTESIAN_POINT('Ctrl Pts',(10.4360539003264,-0.562343168052488,
339.887918759286));
#68275=CARTESIAN_POINT('Ctrl Pts',(10.4282960893514,-0.425757240810356,
339.899787121335));
#68276=CARTESIAN_POINT('Ctrl Pts',(10.4205441163737,-0.289274098784777,
339.911646552066));
#68277=CARTESIAN_POINT('Ctrl Pts',(10.412792143396,-0.152188918465723,339.917808294333));
#68278=CARTESIAN_POINT('Ctrl Pts',(10.4050401704183,-0.015015127859537,
339.918227079796));
#68279=CARTESIAN_POINT('Ctrl Pts',(10.3972914804014,0.122100569643539,339.918645687903));
#68280=CARTESIAN_POINT('Ctrl Pts',(10.3895427903844,0.259304412737212,339.913326175376));
#68281=CARTESIAN_POINT('Ctrl Pts',(10.3817941003674,0.396080507702657,339.902275318045));
#68282=CARTESIAN_POINT('Ctrl Pts',(10.3740470225274,0.532828145308602,339.891226759934));
#68283=CARTESIAN_POINT('Ctrl Pts',(10.3662999446873,0.66914782244632,339.874449260349));
#68284=CARTESIAN_POINT('Ctrl Pts',(10.3585528668472,0.804526703805565,339.852001632869));
#68285=CARTESIAN_POINT('Ctrl Pts',(10.3508057240757,0.939906719829884,339.829553817247));
#68286=CARTESIAN_POINT('Ctrl Pts',(10.3430585813042,1.07434553873882,339.80143584288));
#68287=CARTESIAN_POINT('Ctrl Pts',(10.3353114385327,1.20733887387551,339.767757953811));
#68288=CARTESIAN_POINT('Ctrl Pts',(10.327562554035,1.34036210880657,339.73407249322));
#68289=CARTESIAN_POINT('Ctrl Pts',(10.3198136695374,1.47193883445901,339.69482472652));
#68290=CARTESIAN_POINT('Ctrl Pts',(10.3120647850397,1.6015787046038,339.650175127397));
#68291=CARTESIAN_POINT('Ctrl Pts',(10.3043076757863,1.73135617600836,339.605478136672));
#68292=CARTESIAN_POINT('Ctrl Pts',(10.2965505665329,1.85919231509715,339.55536798767));
#68293=CARTESIAN_POINT('Ctrl Pts',(10.2887934572794,1.98461507483902,339.500054007145));
#68294=CARTESIAN_POINT('Ctrl Pts',(10.2810322028704,2.11010485656511,339.444710468566));
#68295=CARTESIAN_POINT('Ctrl Pts',(10.2732709484614,2.23317833868694,339.384157730011));
#68296=CARTESIAN_POINT('Ctrl Pts',(10.2655096940523,2.35338787257247,339.318651245902));
#68297=CARTESIAN_POINT('Ctrl Pts',(10.2577360241525,2.47378970273879,339.253039972656));
#68298=CARTESIAN_POINT('Ctrl Pts',(10.2499623542528,2.59131809442937,339.182459319926));
#68299=CARTESIAN_POINT('Ctrl Pts',(10.242188684353,2.70555344950424,339.107208735184));
#68300=CARTESIAN_POINT('Ctrl Pts',(10.2347768742993,2.81447121474806,339.035461021721));
#68301=CARTESIAN_POINT('Ctrl Pts',(10.2273650642456,2.92039538667276,338.95946852315));
#68302=CARTESIAN_POINT('Ctrl Pts',(10.219953254192,3.0229915839452,338.879523804012));
#68303=CARTESIAN_POINT('Ctrl Pts',(10.2121781755366,3.13061623942886,338.795660823866));
#68304=CARTESIAN_POINT('Ctrl Pts',(10.2044030968812,3.23491856376309,338.707183391269));
#68305=CARTESIAN_POINT('Ctrl Pts',(10.1966280182258,3.33547737264277,338.614384284922));
#68306=CARTESIAN_POINT('Ctrl Pts',(10.1888625073048,3.43591243744065,338.521699373843));
#68307=CARTESIAN_POINT('Ctrl Pts',(10.1810969963838,3.53261286816526,338.424703633052));
#68308=CARTESIAN_POINT('Ctrl Pts',(10.1733314854627,3.62518844687318,338.323731605764));
#68309=CARTESIAN_POINT('Ctrl Pts',(10.1655736740732,3.71767223656734,338.222859692599));
#68310=CARTESIAN_POINT('Ctrl Pts',(10.1578158626838,3.80603905073919,338.118019624991));
#68311=CARTESIAN_POINT('Ctrl Pts',(10.1500580512943,3.88993389396859,338.009584250865));
#68312=CARTESIAN_POINT('Ctrl Pts',(10.1423060779085,3.97376560361783,337.901230477861));
#68313=CARTESIAN_POINT('Ctrl Pts',(10.1345541045227,4.05313180257354,337.789287091577));
#68314=CARTESIAN_POINT('Ctrl Pts',(10.1268021311369,4.1277165783379,337.674161347304));
#68315=CARTESIAN_POINT('Ctrl Pts',(10.1190534407229,4.20226976734376,337.559084358947));
#68316=CARTESIAN_POINT('Ctrl Pts',(10.1113047503089,4.27204534853561,337.440828020513));
#68317=CARTESIAN_POINT('Ctrl Pts',(10.1035560598949,4.33676984012755,337.319829824849));
#68318=CARTESIAN_POINT('Ctrl Pts',(10.0958089816645,4.40148086521617,337.198856803931));
#68319=CARTESIAN_POINT('Ctrl Pts',(10.0880619034341,4.46114270681581,337.075143404929));
#68320=CARTESIAN_POINT('Ctrl Pts',(10.0803148252037,4.51552729787316,336.949152709426));
#68321=CARTESIAN_POINT('Ctrl Pts',(10.072567682049,4.56991234469991,336.823160958059));
#68322=CARTESIAN_POINT('Ctrl Pts',(10.0648205388942,4.61901989786494,336.694892230992));
#68323=CARTESIAN_POINT('Ctrl Pts',(10.0570733957395,4.66266976545344,336.564830253039));
#68324=CARTESIAN_POINT('Ctrl Pts',(10.0493245108661,4.70632944643928,336.434739034451));
#68325=CARTESIAN_POINT('Ctrl Pts',(10.0415756259925,4.74452887591398,336.302854133222));
#68326=CARTESIAN_POINT('Ctrl Pts',(10.033826741119,4.77713764510589,336.16967473351));
#68327=CARTESIAN_POINT('Ctrl Pts',(10.0260696315036,4.80978102556353,336.036353975884));
#68328=CARTESIAN_POINT('Ctrl Pts',(10.0183125218881,4.83682179894804,335.901736355353));
#68329=CARTESIAN_POINT('Ctrl Pts',(10.0105554122726,4.85818054082088,335.766332105088));
#68330=CARTESIAN_POINT('Ctrl Pts',(10.0027941575084,4.87955069611507,335.630855499169));
#68331=CARTESIAN_POINT('Ctrl Pts',(9.99503290274435,4.89523272514184,335.494591814046));
#68332=CARTESIAN_POINT('Ctrl Pts',(9.98727164798021,4.90519919657519,335.35805572809));
#68333=CARTESIAN_POINT('Ctrl Pts',(9.97949797774061,4.91518161111121,335.221301228942));
#68334=CARTESIAN_POINT('Ctrl Pts',(9.97172430750101,4.91943018545769,335.084273849091));
#68335=CARTESIAN_POINT('Ctrl Pts',(9.96395063726141,4.91796966271429,334.947488485816));
#68336=CARTESIAN_POINT('Ctrl Pts',(9.95653883148027,4.91657712732504,334.817070483117));
#68337=CARTESIAN_POINT('Ctrl Pts',(9.94912702569913,4.90999506239017,334.686872759848));
#68338=CARTESIAN_POINT('Ctrl Pts',(9.941715219918,4.8982885385814,334.557334827096));
#68339=CARTESIAN_POINT('Ctrl Pts',(9.93394013893002,4.88600824233666,334.421447845178));
#68340=CARTESIAN_POINT('Ctrl Pts',(9.92616505794206,4.86804964710762,334.285857538581));
#68341=CARTESIAN_POINT('Ctrl Pts',(9.91838997695407,4.84443102997917,334.151076529789));
#68342=CARTESIAN_POINT('Ctrl Pts',(9.9106244636881,4.82084147703193,334.016461377433));
#68343=CARTESIAN_POINT('Ctrl Pts',(9.90285895042208,4.79160582738062,333.882653922671));
#68344=CARTESIAN_POINT('Ctrl Pts',(9.89509343715611,4.75679423645525,333.750163348863));
#68345=CARTESIAN_POINT('Ctrl Pts',(9.88733562341187,4.72201716129104,333.61780413972));
#68346=CARTESIAN_POINT('Ctrl Pts',(9.87957780966763,4.68167524568344,333.486759588742));
#68347=CARTESIAN_POINT('Ctrl Pts',(9.8718199959234,4.63588991723467,333.357529988772));
#68348=CARTESIAN_POINT('Ctrl Pts',(9.86406802017565,4.59013904367161,333.228397638102));
#68349=CARTESIAN_POINT('Ctrl Pts',(9.85631604442789,4.53895304083585,333.101077886818));
#68350=CARTESIAN_POINT('Ctrl Pts',(9.84856406868013,4.4825034202272,332.976056781886));
#68351=CARTESIAN_POINT('Ctrl Pts',(9.84081537590146,4.42607770608643,332.85108862351));
#68352=CARTESIAN_POINT('Ctrl Pts',(9.83306668312281,4.36439296830595,332.728417530807));
#68353=CARTESIAN_POINT('Ctrl Pts',(9.82531799034413,4.29766910747938,332.608510233115));
#68354=CARTESIAN_POINT('Ctrl Pts',(9.81757090974782,4.23095912912753,332.48862788317));
#68355=CARTESIAN_POINT('Ctrl Pts',(9.80982382915152,4.15921230307949,332.371508525797));
#68356=CARTESIAN_POINT('Ctrl Pts',(9.80207674855521,4.08269462455298,332.257594547638));
#68357=CARTESIAN_POINT('Ctrl Pts',(9.79432960303557,4.00617630478068,332.143679614838));
#68358=CARTESIAN_POINT('Ctrl Pts',(9.78658245751594,3.92488727073439,332.032970439301));
#68359=CARTESIAN_POINT('Ctrl Pts',(9.77883531199629,3.83913678494635,331.925880319673));
#68360=CARTESIAN_POINT('Ctrl Pts',(9.77108642476111,3.75336702070884,331.818766124013));
#68361=CARTESIAN_POINT('Ctrl Pts',(9.76333753752587,3.66313405308759,331.715272908363));
#68362=CARTESIAN_POINT('Ctrl Pts',(9.75558865029069,3.56878708521855,331.615780473598));
#68363=CARTESIAN_POINT('Ctrl Pts',(9.74783153833195,3.47433997681248,331.516182436862));
#68364=CARTESIAN_POINT('Ctrl Pts',(9.74007442637327,3.37577041479077,331.420593947781));
#68365=CARTESIAN_POINT('Ctrl Pts',(9.73231731441453,3.27346448418863,331.329357912673));
#68366=CARTESIAN_POINT('Ctrl Pts',(9.72455605731347,3.17110388470388,331.238073124066));
#68367=CARTESIAN_POINT('Ctrl Pts',(9.71679480021239,3.06500324045312,331.151145671403));
#68368=CARTESIAN_POINT('Ctrl Pts',(9.70903354311133,2.95558051099265,331.068877144436));
#68369=CARTESIAN_POINT('Ctrl Pts',(9.70125987056932,2.8459827414042,330.986477015072));
#68370=CARTESIAN_POINT('Ctrl Pts',(9.6934861980273,2.73305258933912,330.908750925908));
#68371=CARTESIAN_POINT('Ctrl Pts',(9.68571252548529,2.61723643301779,330.835956710578));
#68372=CARTESIAN_POINT('Ctrl Pts',(9.67830074553823,2.50681193798943,330.766551329462));
#68373=CARTESIAN_POINT('Ctrl Pts',(9.67088896559113,2.39376434723797,330.701629109301));
#68374=CARTESIAN_POINT('Ctrl Pts',(9.66347718564407,2.27849846405012,330.641373173599));
#68375=CARTESIAN_POINT('Ctrl Pts',(9.65570211094242,2.15758272468133,330.578163741499));
#68376=CARTESIAN_POINT('Ctrl Pts',(9.6479270362408,2.03384361502961,330.519889851457));
#68377=CARTESIAN_POINT('Ctrl Pts',(9.64015196153915,1.90772210024274,330.466813543351));
#68378=CARTESIAN_POINT('Ctrl Pts',(9.63238645456454,1.78175578605197,330.413802549039));
#68379=CARTESIAN_POINT('Ctrl Pts',(9.6246209475899,1.65341325680026,330.365976560709));
#68380=CARTESIAN_POINT('Ctrl Pts',(9.6168554406153,1.52316065999553,330.323552131549));
#68381=CARTESIAN_POINT('Ctrl Pts',(9.60909763316098,1.39303720897802,330.28116976632));
#68382=CARTESIAN_POINT('Ctrl Pts',(9.60133982570669,1.26100782851349,330.244178422469));
#68383=CARTESIAN_POINT('Ctrl Pts',(9.59358201825236,1.12755893623701,330.212746726168));
#68384=CARTESIAN_POINT('Ctrl Pts',(9.5858300487866,0.994210468353891,330.181338683185));
#68385=CARTESIAN_POINT('Ctrl Pts',(9.5780780793208,0.859444993842858,330.155482049344));
#68386=CARTESIAN_POINT('Ctrl Pts',(9.57032610985505,0.723764053976697,330.135295624946));
#68387=CARTESIAN_POINT('Ctrl Pts',(9.56257742332448,0.588140574570665,330.115117749437));
#68388=CARTESIAN_POINT('Ctrl Pts',(9.55482873679395,0.451602786725605,330.100605364723));
#68389=CARTESIAN_POINT('Ctrl Pts',(9.54708005026339,0.314662173250379,330.091826125816));
#68390=CARTESIAN_POINT('Ctrl Pts',(9.53933297589371,0.177750051094268,330.083048713481));
#68391=CARTESIAN_POINT('Ctrl Pts',(9.53158590152403,0.0404356598416378,
330.08000209935));
#68392=CARTESIAN_POINT('Ctrl Pts',(9.52383882715435,-0.0967650435309119,
330.082702003249));
#68393=CARTESIAN_POINT('Ctrl Pts',(9.51609168783409,-0.233966897178491,
330.085401929784));
#68394=CARTESIAN_POINT('Ctrl Pts',(9.50834454851381,-0.371054670245795,
330.093848462754));
#68395=CARTESIAN_POINT('Ctrl Pts',(9.50059740919355,-0.507513452040183,
330.108005196395));
#68396=CARTESIAN_POINT('Ctrl Pts',(9.49284852812469,-0.644002913144896,
330.12216511282));
#68397=CARTESIAN_POINT('Ctrl Pts',(9.48509964705582,-0.779862712868882,
330.142037744198));
#68398=CARTESIAN_POINT('Ctrl Pts',(9.47735076598696,-0.914584495363758,
330.167534970293));
#68399=CARTESIAN_POINT('Ctrl Pts',(9.46959366010778,-1.04944927413084,330.193059259631));
#68400=CARTESIAN_POINT('Ctrl Pts',(9.46183655422864,-1.18317323808522,330.224219996623));
#68401=CARTESIAN_POINT('Ctrl Pts',(9.45407944834946,-1.31525909789341,330.260878080498));
#68402=CARTESIAN_POINT('Ctrl Pts',(9.44631819729033,-1.44741554068276,330.297555753424));
#68403=CARTESIAN_POINT('Ctrl Pts',(9.43855694623125,-1.5779317633539,330.339736506579));
#68404=CARTESIAN_POINT('Ctrl Pts',(9.43079569517212,-1.70632797144456,330.387232076468));
#68405=CARTESIAN_POINT('Ctrl Pts',(9.42302202854694,-1.83492957317483,330.434803624363));
#68406=CARTESIAN_POINT('Ctrl Pts',(9.4152483619217,-1.96140402259827,330.487706827669));
#68407=CARTESIAN_POINT('Ctrl Pts',(9.40747469529651,-2.08529294175604,330.545705846089));
#68408=CARTESIAN_POINT('Ctrl Pts',(9.40006284732105,-2.20341555736534,330.601005349912));
#68409=CARTESIAN_POINT('Ctrl Pts',(9.3926509993456,-2.31918765281013,330.660936851974));
#68410=CARTESIAN_POINT('Ctrl Pts',(9.38523915137014,-2.43223616300396,330.725259035933));
#68411=CARTESIAN_POINT('Ctrl Pts',(9.37746407213797,-2.55082482358454,330.792733446946));
#68412=CARTESIAN_POINT('Ctrl Pts',(9.36968899290579,-2.66679096589698,330.865252999787));
#68413=CARTESIAN_POINT('Ctrl Pts',(9.36191391367362,-2.77967560314094,330.942588681955));
#68414=CARTESIAN_POINT('Ctrl Pts',(9.35414840220223,-2.89242132820501,331.019829197336));
#68415=CARTESIAN_POINT('Ctrl Pts',(9.3463828907308,-3.00209277381689,331.101873831063));
#68416=CARTESIAN_POINT('Ctrl Pts',(9.3386173792594,-3.10825557629554,331.188447778801));
#68417=CARTESIAN_POINT('Ctrl Pts',(9.33085956734618,-3.21431311762354,331.274935887873));
#68418=CARTESIAN_POINT('Ctrl Pts',(9.32310175543299,-3.31686863794535,331.365944128484));
#68419=CARTESIAN_POINT('Ctrl Pts',(9.31534394351976,-3.41551710710683,331.461154714662));
#68420=CARTESIAN_POINT('Ctrl Pts',(9.30759196963713,-3.51409133977126,331.556293651473));
#68421=CARTESIAN_POINT('Ctrl Pts',(9.29983999575445,-3.60876409347624,331.655628368866));
#68422=CARTESIAN_POINT('Ctrl Pts',(9.29208802187182,-3.69916405343823,331.758801399443));
#68423=CARTESIAN_POINT('Ctrl Pts',(9.28433933100309,-3.78952572839959,331.861930735538));
#68424=CARTESIAN_POINT('Ctrl Pts',(9.27659064013434,-3.87561795164439,331.968894858332));
#68425=CARTESIAN_POINT('Ctrl Pts',(9.26884194926561,-3.9571070376224,332.079300262728));
#68426=CARTESIAN_POINT('Ctrl Pts',(9.26109487060617,-4.0385791688059,332.189682695938));
#68427=CARTESIAN_POINT('Ctrl Pts',(9.25334779194675,-4.11544983575781,332.303504672284));
#68428=CARTESIAN_POINT('Ctrl Pts',(9.2456007132873,-4.18742660509345,332.420340819128));
#68429=CARTESIAN_POINT('Ctrl Pts',(9.23785356972949,-4.25940397738855,332.537177944725));
#68430=CARTESIAN_POINT('Ctrl Pts',(9.23010642617165,-4.32648716527949,332.657028958392));
#68431=CARTESIAN_POINT('Ctrl Pts',(9.22235928261384,-4.3884281350977,332.779441159171));
#68432=CARTESIAN_POINT('Ctrl Pts',(9.21461039736349,-4.45038303032262,332.901880880341));
#68433=CARTESIAN_POINT('Ctrl Pts',(9.20686151211319,-4.50719323060179,333.026882585701));
#68434=CARTESIAN_POINT('Ctrl Pts',(9.19911262686284,-4.55865773726159,333.153971100712));
#68435=CARTESIAN_POINT('Ctrl Pts',(9.1913555169137,-4.61017686856121,333.281194507999));
#68436=CARTESIAN_POINT('Ctrl Pts',(9.18359840696458,-4.65633882506793,333.410508786635));
#68437=CARTESIAN_POINT('Ctrl Pts',(9.17584129701544,-4.69699146744889,333.54142047964));
#68438=CARTESIAN_POINT('Ctrl Pts',(9.16808004194063,-4.73766583316658,333.672402127232));
#68439=CARTESIAN_POINT('Ctrl Pts',(9.16031878686583,-4.7728249184651,333.804982512447));
#68440=CARTESIAN_POINT('Ctrl Pts',(9.15255753179102,-4.80236739346133,333.938656285306));
#68441=CARTESIAN_POINT('Ctrl Pts',(9.14478386128284,-4.83195712661703,334.072543891857));
#68442=CARTESIAN_POINT('Ctrl Pts',(9.13701019077465,-4.85591222701698,334.207527996125));
#68443=CARTESIAN_POINT('Ctrl Pts',(9.12923652026646,-4.8741829628194,334.343095511158));
#68444=CARTESIAN_POINT('Ctrl Pts',(9.12182471920972,-4.89160318390869,334.472352269612));
#68445=CARTESIAN_POINT('Ctrl Pts',(9.11441291815298,-4.90385632254623,334.602139058645));
#68446=CARTESIAN_POINT('Ctrl Pts',(9.10700111709625,-4.91094341938446,334.732011578413));
#68447=CARTESIAN_POINT('Ctrl Pts',(9.10193987023375,-4.91578293765565,334.820696754684));
#68448=CARTESIAN_POINT('Ctrl Pts',(9.09687862337123,-4.91822036105881,334.90951420329));
#68449=CARTESIAN_POINT('Ctrl Pts',(9.09181737650877,-4.91824973135267,334.998374407977));
#68450=CARTESIAN_POINT('',(7.34181737656206,-4.91824863900072,334.996341111162));
#68451=CARTESIAN_POINT('Ctrl Pts',(9.09181737647953,-4.91824973135284,334.998374408491));
#68452=CARTESIAN_POINT('Ctrl Pts',(9.08410754254342,-4.91829447131967,335.13373580071));
#68453=CARTESIAN_POINT('Ctrl Pts',(9.07639770860732,-4.91274680624549,335.269324293168));
#68454=CARTESIAN_POINT('Ctrl Pts',(9.06868787467121,-4.9015766619707,335.4046347604));
#68455=CARTESIAN_POINT('Ctrl Pts',(9.06098726770942,-4.89041988590009,335.539783290785));
#68456=CARTESIAN_POINT('Ctrl Pts',(9.05328666074762,-4.87365404750714,335.674654064992));
#68457=CARTESIAN_POINT('Ctrl Pts',(9.04558605378583,-4.85130105419687,335.808740467671));
#68458=CARTESIAN_POINT('Ctrl Pts',(9.03789274498896,-4.82896924568837,335.942699791447));
#68459=CARTESIAN_POINT('Ctrl Pts',(9.03019943619208,-4.80106088196502,336.075875832535));
#68460=CARTESIAN_POINT('Ctrl Pts',(9.02250612739522,-4.76764975578662,336.207766065365));
#68461=CARTESIAN_POINT('Ctrl Pts',(9.01443350053801,-4.73259129633322,336.346159137041));
#68462=CARTESIAN_POINT('Ctrl Pts',(9.00636087368077,-4.69147366052708,336.483135933379));
#68463=CARTESIAN_POINT('Ctrl Pts',(8.99828824682356,-4.64444300410043,336.618126152116));
#68464=CARTESIAN_POINT('Ctrl Pts',(8.99060304167977,-4.599669444133,336.746637916843));
#68465=CARTESIAN_POINT('Ctrl Pts',(8.98291783653599,-4.54953734429063,336.873348920796));
#68466=CARTESIAN_POINT('Ctrl Pts',(8.9752326313922,-4.49422406301,336.997782053669));
#68467=CARTESIAN_POINT('Ctrl Pts',(8.96754842408633,-4.4389179635402,337.122199030292));
#68468=CARTESIAN_POINT('Ctrl Pts',(8.9598642167805,-4.37843218198699,337.24433836039));
#68469=CARTESIAN_POINT('Ctrl Pts',(8.95218000947463,-4.31299201024085,337.363743425607));
#68470=CARTESIAN_POINT('Ctrl Pts',(8.9444950684509,-4.24754559001375,337.483159892081));
#68471=CARTESIAN_POINT('Ctrl Pts',(8.9368101274272,-4.17714403006146,337.599841225438));
#68472=CARTESIAN_POINT('Ctrl Pts',(8.92912518640347,-4.10205807164927,337.713356342119));
#68473=CARTESIAN_POINT('Ctrl Pts',(8.92143777987631,-4.02694802395825,337.826907877024));
#68474=CARTESIAN_POINT('Ctrl Pts',(8.91375037334906,-3.94715080806605,337.937290843134));
#68475=CARTESIAN_POINT('Ctrl Pts',(8.90606296682191,-3.86297958756368,338.044104428));
#68476=CARTESIAN_POINT('Ctrl Pts',(8.89836717245813,-3.7787165266671,338.15103455866));
#68477=CARTESIAN_POINT('Ctrl Pts',(8.89067137809435,-3.69007018080346,338.254387221121));
#68478=CARTESIAN_POINT('Ctrl Pts',(8.88297558373057,-3.59739318926874,338.353795656313));
#68479=CARTESIAN_POINT('Ctrl Pts',(8.8752748898708,-3.50465719530665,338.453267379479));
#68480=CARTESIAN_POINT('Ctrl Pts',(8.86757419601105,-3.40788572869358,338.548789596827));
#68481=CARTESIAN_POINT('Ctrl Pts',(8.85987350215129,-3.30746624117089,338.640034357807));
#68482=CARTESIAN_POINT('Ctrl Pts',(8.85216184201642,-3.20690374994678,338.731409057097));
#68483=CARTESIAN_POINT('Ctrl Pts',(8.84445018188164,-3.10268317295261,338.818493887959));
#68484=CARTESIAN_POINT('Ctrl Pts',(8.83673852174678,-2.99522304385326,338.901002689062));
#68485=CARTESIAN_POINT('Ctrl Pts',(8.83408004210527,-2.95817776949094,338.929446365799));
#68486=CARTESIAN_POINT('Ctrl Pts',(8.83142156246372,-2.92074773267013,338.957346608124));
#68487=CARTESIAN_POINT('Ctrl Pts',(8.82876308282221,-2.88295077582512,338.984692947602));
#68488=CARTESIAN_POINT('Ctrl Pts',(8.82098803347039,-2.77240894573939,339.064670667089));
#68489=CARTESIAN_POINT('Ctrl Pts',(8.81321298411855,-2.65836184263739,339.140171372476));
#68490=CARTESIAN_POINT('Ctrl Pts',(8.80543793476673,-2.54120805372173,339.210872200649));
#68491=CARTESIAN_POINT('Ctrl Pts',(8.79767245314615,-2.42419843057469,339.281486026606));
#68492=CARTESIAN_POINT('Ctrl Pts',(8.78990697152558,-2.30409005972581,339.347311527713));
#68493=CARTESIAN_POINT('Ctrl Pts',(8.782141489905,-2.18131300429889,339.408067222693));
#68494=CARTESIAN_POINT('Ctrl Pts',(8.77438370778293,-2.05865768269373,339.468762678217));
#68495=CARTESIAN_POINT('Ctrl Pts',(8.76662592566089,-1.93333929029083,339.524398158843));
#68496=CARTESIAN_POINT('Ctrl Pts',(8.75886814353882,-1.80581485692351,339.574736688053));
#68497=CARTESIAN_POINT('Ctrl Pts',(8.75111619935774,-1.67838638914334,339.625037336156));
#68498=CARTESIAN_POINT('Ctrl Pts',(8.74336425517663,-1.54875554686997,339.670048824038));
#68499=CARTESIAN_POINT('Ctrl Pts',(8.73561231099555,-1.41740150757175,339.709581300799));
#68500=CARTESIAN_POINT('Ctrl Pts',(8.72786364958949,-1.28610309377204,339.74909703644));
#68501=CARTESIAN_POINT('Ctrl Pts',(8.72011498818342,-1.15308330785384,339.783138263336));
#68502=CARTESIAN_POINT('Ctrl Pts',(8.71236632677736,-1.01883853709875,339.811564308811));
#68503=CARTESIAN_POINT('Ctrl Pts',(8.7046192774313,-0.884621695119256,339.839984440427));
#68504=CARTESIAN_POINT('Ctrl Pts',(8.69687222808524,-0.74918075737672,339.862791633339));
#68505=CARTESIAN_POINT('Ctrl Pts',(8.68912517873918,-0.613024024494354,
339.879895962814));
#68506=CARTESIAN_POINT('Ctrl Pts',(8.68137806431856,-0.476866147907073,
339.897000435965));
#68507=CARTESIAN_POINT('Ctrl Pts',(8.67363094989797,-0.339992852016731,
339.908401901411));
#68508=CARTESIAN_POINT('Ctrl Pts',(8.66588383547736,-0.202918915392262,
339.914062166505));
#68509=CARTESIAN_POINT('Ctrl Pts',(8.65813497916096,-0.0658141584519695,
339.919723704278));
#68510=CARTESIAN_POINT('Ctrl Pts',(8.65038612284457,0.0714909385238468,
339.919641456873));
#68511=CARTESIAN_POINT('Ctrl Pts',(8.64263726652817,0.208480629353462,339.913829350892));
#68512=CARTESIAN_POINT('Ctrl Pts',(8.63488018503037,0.345615730681223,339.908011075533));
#68513=CARTESIAN_POINT('Ctrl Pts',(8.62712310353256,0.482434365936827,339.896450808678));
#68514=CARTESIAN_POINT('Ctrl Pts',(8.61936602203477,0.618424391671335,339.879214520216));
#68515=CARTESIAN_POINT('Ctrl Pts',(8.61160479519355,0.754487089758085,339.861969020772));
#68516=CARTESIAN_POINT('Ctrl Pts',(8.60384356835233,0.889719910813559,339.839041521031));
#68517=CARTESIAN_POINT('Ctrl Pts',(8.59608234151111,1.02362093744717,339.810549161886));
#68518=CARTESIAN_POINT('Ctrl Pts',(8.58830869858097,1.15773617339159,339.782011221845));
#68519=CARTESIAN_POINT('Ctrl Pts',(8.58053505565073,1.29051497866879,339.747890730042));
#68520=CARTESIAN_POINT('Ctrl Pts',(8.57276141272058,1.42146977119236,339.708354994272));
#68521=CARTESIAN_POINT('Ctrl Pts',(8.56534929132981,1.54633437169053,339.670657909979));
#68522=CARTESIAN_POINT('Ctrl Pts',(8.55793716993905,1.66954052761693,339.628038032801));
#68523=CARTESIAN_POINT('Ctrl Pts',(8.55052504854828,1.79068424137417,339.580680409087));
#68524=CARTESIAN_POINT('Ctrl Pts',(8.5427499581479,1.91776032070997,339.531003698992));
#68525=CARTESIAN_POINT('Ctrl Pts',(8.53497486774757,2.04296846105325,339.475956514327));
#68526=CARTESIAN_POINT('Ctrl Pts',(8.52719977734719,2.16582145814549,339.415699318787));
#68527=CARTESIAN_POINT('Ctrl Pts',(8.5194342548707,2.28852327395677,339.355516274958));
#68528=CARTESIAN_POINT('Ctrl Pts',(8.51166873239421,2.40887536554206,339.290136147524));
#68529=CARTESIAN_POINT('Ctrl Pts',(8.50390320991772,2.52640829426202,339.219768262972));
#68530=CARTESIAN_POINT('Ctrl Pts',(8.4961453871716,2.64382468583162,339.149470150124));
#68531=CARTESIAN_POINT('Ctrl Pts',(8.48838756442549,2.75842714409564,339.074194321471));
#68532=CARTESIAN_POINT('Ctrl Pts',(8.48062974167937,2.86976906229912,338.994196864398));
#68533=CARTESIAN_POINT('Ctrl Pts',(8.47287775714514,2.98102718924667,338.914259610056));
#68534=CARTESIAN_POINT('Ctrl Pts',(8.46512577261092,3.08902934403782,338.829608027117));
#68535=CARTESIAN_POINT('Ctrl Pts',(8.45737378807669,3.19335656356526,338.740542329721));
#68536=CARTESIAN_POINT('Ctrl Pts',(8.44962508686652,3.29763959568915,338.651514355768));
#68537=CARTESIAN_POINT('Ctrl Pts',(8.44187638565634,3.39825049167207,338.558076239086));
#68538=CARTESIAN_POINT('Ctrl Pts',(8.43412768444617,3.49480233025679,338.460569279025));
#68539=CARTESIAN_POINT('Ctrl Pts',(8.42638059563513,3.59133407771952,338.363082608834));
#68540=CARTESIAN_POINT('Ctrl Pts',(8.4186335068241,3.68380817296939,338.261529056925));
#68541=CARTESIAN_POINT('Ctrl Pts',(8.41088641801306,3.77187392275263,338.156287403479));
#68542=CARTESIAN_POINT('Ctrl Pts',(8.4031392645021,3.85994040801835,338.051044871105));
#68543=CARTESIAN_POINT('Ctrl Pts',(8.39539211099112,3.94359822354101,337.942114475523));
#68544=CARTESIAN_POINT('Ctrl Pts',(8.38764495748015,4.02253667302524,337.829908439626));
#68545=CARTESIAN_POINT('Ctrl Pts',(8.37989606248383,4.10149286711114,337.717677180895));
#68546=CARTESIAN_POINT('Ctrl Pts',(8.3721471674875,4.17572735928963,337.602169136254));
#68547=CARTESIAN_POINT('Ctrl Pts',(8.36439827249117,4.2449727577381,337.483825547127));
#68548=CARTESIAN_POINT('Ctrl Pts',(8.35664115317578,4.3142916500526,337.365356353583));
#68549=CARTESIAN_POINT('Ctrl Pts',(8.3488840338604,4.37861067327945,337.244045941661));
#68550=CARTESIAN_POINT('Ctrl Pts',(8.34112691454501,4.43770814948298,337.120360686891));
#68551=CARTESIAN_POINT('Ctrl Pts',(8.33336565029588,4.49683720379094,336.996609342228));
#68552=CARTESIAN_POINT('Ctrl Pts',(8.3256043860467,4.55073899806773,336.870480985421));
#68553=CARTESIAN_POINT('Ctrl Pts',(8.31784312179755,4.59924041896377,336.742461084521));
#68554=CARTESIAN_POINT('Ctrl Pts',(8.3100694425331,4.64781942333895,336.614236401387));
#68555=CARTESIAN_POINT('Ctrl Pts',(8.30229576326871,4.6909806689184,336.484114499033));
#68556=CARTESIAN_POINT('Ctrl Pts',(8.29452208400426,4.72860098635664,336.352595939047));
#68557=CARTESIAN_POINT('Ctrl Pts',(8.2871103940943,4.7644694750968,336.227201675809));
#68558=CARTESIAN_POINT('Ctrl Pts',(8.27969870418431,4.79530138581858,336.100538179217));
#68559=CARTESIAN_POINT('Ctrl Pts',(8.27228701427435,4.82103370919337,335.973045239093));
#68560=CARTESIAN_POINT('Ctrl Pts',(8.26451185432889,4.84802794835314,335.839300032072));
#68561=CARTESIAN_POINT('Ctrl Pts',(8.25673669438341,4.86949507726135,335.704219350032));
#68562=CARTESIAN_POINT('Ctrl Pts',(8.24896153443794,4.88530638429945,335.568299739594));
#68563=CARTESIAN_POINT('Ctrl Pts',(8.24119594181795,4.90109823554221,335.432547378083));
#68564=CARTESIAN_POINT('Ctrl Pts',(8.23343034919796,4.91124806756337,335.295958526694));
#68565=CARTESIAN_POINT('Ctrl Pts',(8.22566475657797,4.91567787271867,335.159041234163));
#68566=CARTESIAN_POINT('Ctrl Pts',(8.21790686316969,4.92010328593513,335.022259688545));
#68567=CARTESIAN_POINT('Ctrl Pts',(8.21014896976141,4.91881994560553,334.88515073796));
#68568=CARTESIAN_POINT('Ctrl Pts',(8.20239107635314,4.91180152206862,334.748228535564));
#68569=CARTESIAN_POINT('Ctrl Pts',(8.19463902071675,4.90478837985661,334.611409366368));
#68570=CARTESIAN_POINT('Ctrl Pts',(8.18688696508037,4.89204876439694,334.474777054429));
#68571=CARTESIAN_POINT('Ctrl Pts',(8.17913490944397,4.87360841273638,334.338846385622));
#68572=CARTESIAN_POINT('Ctrl Pts',(8.17138613671882,4.85517587036418,334.202973281974));
#68573=CARTESIAN_POINT('Ctrl Pts',(8.16363736399368,4.83104744590153,334.067801616982));
#68574=CARTESIAN_POINT('Ctrl Pts',(8.15588859126854,4.8013007654651,333.933841464864));
#68575=CARTESIAN_POINT('Ctrl Pts',(8.148141430702,4.77156027392707,333.799909183612));
#68576=CARTESIAN_POINT('Ctrl Pts',(8.14039427013551,4.7362039361131,333.667188295201));
#68577=CARTESIAN_POINT('Ctrl Pts',(8.13264710956898,4.69536050153297,333.536178691525));
#68578=CARTESIAN_POINT('Ctrl Pts',(8.12489988413112,4.65451672494779,333.405167990833));
#68579=CARTESIAN_POINT('Ctrl Pts',(8.11715265869318,4.60818587628597,333.27586897661));
#68580=CARTESIAN_POINT('Ctrl Pts',(8.10940543325532,4.55654647229255,333.148766003894));
#68581=CARTESIAN_POINT('Ctrl Pts',(8.10165646622969,4.50489545968457,333.021634458242));
#68582=CARTESIAN_POINT('Ctrl Pts',(8.09390749920413,4.44793366416211,332.896700298501));
#68583=CARTESIAN_POINT('Ctrl Pts',(8.0861585321785,4.38588743921164,332.774427167432));
#68584=CARTESIAN_POINT('Ctrl Pts',(8.0784013410826,4.32377536386944,332.652024266444));
#68585=CARTESIAN_POINT('Ctrl Pts',(8.0706441499867,4.25656825690343,332.532288384802));
#68586=CARTESIAN_POINT('Ctrl Pts',(8.0628869588908,4.18453834592537,332.415658324838));
#68587=CARTESIAN_POINT('Ctrl Pts',(8.05512562288319,4.11246994709544,332.298965945757));
#68588=CARTESIAN_POINT('Ctrl Pts',(8.04736428687552,4.03557382840571,332.185383018638));
#68589=CARTESIAN_POINT('Ctrl Pts',(8.0396029508679,3.95416455384308,332.07531783887));
#68590=CARTESIAN_POINT('Ctrl Pts',(8.03182920061177,3.87262506523414,331.965076609966));
#68591=CARTESIAN_POINT('Ctrl Pts',(8.0240554503557,3.78655824098585,331.858364676495));
#68592=CARTESIAN_POINT('Ctrl Pts',(8.01628170009957,3.69631836510102,331.755556502832));
#68593=CARTESIAN_POINT('Ctrl Pts',(8.00887079339987,3.61029047910769,331.657546950443));
#68594=CARTESIAN_POINT('Ctrl Pts',(8.00145988670013,3.52047050468999,331.563085172389));
#68595=CARTESIAN_POINT('Ctrl Pts',(7.99404898000043,3.42719405997353,331.472462057216));
#68596=CARTESIAN_POINT('Ctrl Pts',(7.98627410851617,3.32933661829125,331.377388255517));
#68597=CARTESIAN_POINT('Ctrl Pts',(7.97849923703191,3.22736533653725,331.286239256395));
#68598=CARTESIAN_POINT('Ctrl Pts',(7.97072436554765,3.12162808045917,331.199391997352));
#68599=CARTESIAN_POINT('Ctrl Pts',(7.96295906192474,3.01602094606957,331.112651613714));
#68600=CARTESIAN_POINT('Ctrl Pts',(7.95519375830186,2.90665735776875,331.030202682796));
#68601=CARTESIAN_POINT('Ctrl Pts',(7.94742845467894,2.79392229422256,330.952385730292));
#68602=CARTESIAN_POINT('Ctrl Pts',(7.93967085050097,2.68129900961734,330.874645934763));
#68603=CARTESIAN_POINT('Ctrl Pts',(7.93191324632298,2.56531122190909,330.801529198564));
#68604=CARTESIAN_POINT('Ctrl Pts',(7.92415564214502,2.44637701059868,330.733335895045));
#68605=CARTESIAN_POINT('Ctrl Pts',(7.91640387567222,2.32753229893818,330.665193907936));
#68606=CARTESIAN_POINT('Ctrl Pts',(7.90865210919945,2.20574591469231,330.601968172642));
#68607=CARTESIAN_POINT('Ctrl Pts',(7.90090034272663,2.08146464707327,330.543915621817));
#68608=CARTESIAN_POINT('Ctrl Pts',(7.89315185805154,1.95723599533002,330.485887648195));
#68609=CARTESIAN_POINT('Ctrl Pts',(7.88540337337647,1.83051491441665,330.433028668135));
#68610=CARTESIAN_POINT('Ctrl Pts',(7.87765488870139,1.7017723127771,330.385549430543));
#68611=CARTESIAN_POINT('Ctrl Pts',(7.86990801546764,1.5730564855533,330.33808006714));
#68612=CARTESIAN_POINT('Ctrl Pts',(7.86216114223388,1.4423203403539,330.295988355972));
#68613=CARTESIAN_POINT('Ctrl Pts',(7.85441426900013,1.31005388964136,330.259436545226));
#68614=CARTESIAN_POINT('Ctrl Pts',(7.84666732991003,1.17778631452862,330.222884423753));
#68615=CARTESIAN_POINT('Ctrl Pts',(7.83892039081992,1.04398878473043,330.191872400757));
#68616=CARTESIAN_POINT('Ctrl Pts',(7.83117345172982,0.909165179699443,330.166512466291));
#68617=CARTESIAN_POINT('Ctrl Pts',(7.82342476979832,0.774311243184096,330.14114682656));
#68618=CARTESIAN_POINT('Ctrl Pts',(7.81567608786683,0.638431156179882,330.121435877864));
#68619=CARTESIAN_POINT('Ctrl Pts',(7.80792740593532,0.502037267884032,330.107440174698));
#68620=CARTESIAN_POINT('Ctrl Pts',(7.80017049635155,0.365498554765905,330.093429610711));
#68621=CARTESIAN_POINT('Ctrl Pts',(7.79241358676781,0.228445340016672,330.085146454658));
#68622=CARTESIAN_POINT('Ctrl Pts',(7.78465667718405,0.0913939089992144,
330.082599241886));
#68623=CARTESIAN_POINT('Ctrl Pts',(7.77689562118348,-0.0457307821677491,
330.080050667515));
#68624=CARTESIAN_POINT('Ctrl Pts',(7.76913456518287,-0.182853297111027,
330.083244136836));
#68625=CARTESIAN_POINT('Ctrl Pts',(7.76137350918231,-0.319460094755516,
330.092136074588));
#68626=CARTESIAN_POINT('Ctrl Pts',(7.7536000335394,-0.45628549764744,330.101042241678));
#68627=CARTESIAN_POINT('Ctrl Pts',(7.74582655789653,-0.592593145221596,
330.115665057905));
#68628=CARTESIAN_POINT('Ctrl Pts',(7.73805308225363,-0.727876451581748,
330.135909238744));
#68629=CARTESIAN_POINT('Ctrl Pts',(7.73063903674461,-0.85690452551417,330.155217368715));
#68630=CARTESIAN_POINT('Ctrl Pts',(7.7232249912356,-0.985000584621647,330.179638587204));
#68631=CARTESIAN_POINT('Ctrl Pts',(7.71581094572659,-1.11173783880216,330.209047898353));
#68632=CARTESIAN_POINT('Ctrl Pts',(7.70803573266196,-1.24464896718422,330.239889853665));
#68633=CARTESIAN_POINT('Ctrl Pts',(7.70026051959734,-1.3764857036768,330.276315585869));
#68634=CARTESIAN_POINT('Ctrl Pts',(7.69248530653272,-1.5067427916735,330.318236526453));
#68635=CARTESIAN_POINT('Ctrl Pts',(7.68471966236776,-1.63683957319427,330.360105875232));
#68636=CARTESIAN_POINT('Ctrl Pts',(7.67695401820283,-1.76536020583765,330.407456857526));
#68637=CARTESIAN_POINT('Ctrl Pts',(7.66918837403787,-1.8918099704092,330.460149991645));
#68638=CARTESIAN_POINT('Ctrl Pts',(7.66143043069044,-2.01813434080322,330.512790872506));
#68639=CARTESIAN_POINT('Ctrl Pts',(7.65367248734299,-2.14239157140488,330.570763213374));
#68640=CARTESIAN_POINT('Ctrl Pts',(7.64591454399556,-2.26410279659415,330.633877969072));
#68641=CARTESIAN_POINT('Ctrl Pts',(7.63816244005857,-2.38572240964241,330.69694521824));
#68642=CARTESIAN_POINT('Ctrl Pts',(7.63041033612161,-2.50479948615676,330.765146998587));
#68643=CARTESIAN_POINT('Ctrl Pts',(7.62265823218462,-2.6208761551355,330.838246614473));
#68644=CARTESIAN_POINT('Ctrl Pts',(7.61490941379342,-2.73690362776522,330.911315248817));
#68645=CARTESIAN_POINT('Ctrl Pts',(7.60716059540217,-2.84993289204024,330.989277382153));
#68646=CARTESIAN_POINT('Ctrl Pts',(7.59941177701097,-2.95953186226359,331.071851044226));
#68647=CARTESIAN_POINT('Ctrl Pts',(7.59166457238506,-3.06910800745674,331.154407509547));
#68648=CARTESIAN_POINT('Ctrl Pts',(7.58391736775921,-3.17525496759558,331.241573358259));
#68649=CARTESIAN_POINT('Ctrl Pts',(7.5761701631333,-3.27757110396192,331.333024308647));
#68650=CARTESIAN_POINT('Ctrl Pts',(7.56842289527597,-3.3798880754159,331.424476005443));
#68651=CARTESIAN_POINT('Ctrl Pts',(7.56067562741865,-3.47837386931059,331.520212613203));
#68652=CARTESIAN_POINT('Ctrl Pts',(7.55292835956132,-3.57266160545297,331.619870991305));
#68653=CARTESIAN_POINT('Ctrl Pts',(7.54517935179048,-3.66697051712582,331.719551751098));
#68654=CARTESIAN_POINT('Ctrl Pts',(7.5374303440196,-3.75707922637368,331.823155749992));
#68655=CARTESIAN_POINT('Ctrl Pts',(7.52968133624876,-3.84265952213,331.930284889524));
#68656=CARTESIAN_POINT('Ctrl Pts',(7.52192410726055,-3.92833061328026,332.037527686439));
#68657=CARTESIAN_POINT('Ctrl Pts',(7.51416687827237,-4.00946344942378,332.148302789043));
#68658=CARTESIAN_POINT('Ctrl Pts',(7.50640964928417,-4.08577143287314,332.262180637657));
#68659=CARTESIAN_POINT('Ctrl Pts',(7.49864827687753,-4.16212017519473,332.376119312577));
#68660=CARTESIAN_POINT('Ctrl Pts',(7.4908869044709,-4.23363872595838,332.493163702452));
#68661=CARTESIAN_POINT('Ctrl Pts',(7.48312553206426,-4.30008579241826,332.612858353523));
#68662=CARTESIAN_POINT('Ctrl Pts',(7.47535174830598,-4.36663911558953,332.732744410486));
#68663=CARTESIAN_POINT('Ctrl Pts',(7.46757796454767,-4.42810457313419,332.855288848026));
#68664=CARTESIAN_POINT('Ctrl Pts',(7.45980418078938,-4.48428811884057,332.98001407685));
#68665=CARTESIAN_POINT('Ctrl Pts',(7.4523937576771,-4.53784554448783,333.098909423967));
#68666=CARTESIAN_POINT('Ctrl Pts',(7.44498333456483,-4.5866035606663,333.219786036243));
#68667=CARTESIAN_POINT('Ctrl Pts',(7.43757291145255,-4.63043647946362,333.342218026352));
#68668=CARTESIAN_POINT('Ctrl Pts',(7.42853293022947,-4.68390829299926,333.491572911345));
#68669=CARTESIAN_POINT('Ctrl Pts',(7.41949294900638,-4.73019051434829,333.643629749562));
#68670=CARTESIAN_POINT('Ctrl Pts',(7.4104529677833,-4.76904131470013,333.79774046014));
#68671=CARTESIAN_POINT('Ctrl Pts',(7.40145047453499,-4.80773100433867,333.951212087707));
#68672=CARTESIAN_POINT('Ctrl Pts',(7.3924479812867,-4.83905068851853,334.106720477118));
#68673=CARTESIAN_POINT('Ctrl Pts',(7.38344548803838,-4.86280821719862,334.263603839468));
#68674=CARTESIAN_POINT('Ctrl Pts',(7.37451337646857,-4.88638000902782,334.419260684445));
#68675=CARTESIAN_POINT('Ctrl Pts',(7.36558126489878,-4.90250734734599,334.576270960164));
#68676=CARTESIAN_POINT('Ctrl Pts',(7.35664915332899,-4.91104982362841,334.733968625273));
#68677=CARTESIAN_POINT('Ctrl Pts',(7.35170522774001,-4.91577808600577,334.821254315309));
#68678=CARTESIAN_POINT('Ctrl Pts',(7.34676130215096,-4.9181834765372,334.90875025729));
#68679=CARTESIAN_POINT('Ctrl Pts',(7.34181737656198,-4.91824863900072,334.996341111162));
#68680=CARTESIAN_POINT('Ctrl Pts',(7.34181737650883,-4.91824863900143,334.996341112105));
#68681=CARTESIAN_POINT('Ctrl Pts',(7.33405948590145,-4.91835089036512,335.133786599567));
#68682=CARTESIAN_POINT('Ctrl Pts',(7.32630159529412,-4.9126872523713,335.271288781228));
#68683=CARTESIAN_POINT('Ctrl Pts',(7.31854370468673,-4.90127022971028,335.408329766066));
#68684=CARTESIAN_POINT('Ctrl Pts',(7.31078659251573,-4.88985435264751,335.545357000041));
#68685=CARTESIAN_POINT('Ctrl Pts',(7.30302948034469,-4.8726862711426,335.681922741711));
#68686=CARTESIAN_POINT('Ctrl Pts',(7.2952723681737,-4.84983049454056,335.817512835816));
#68687=CARTESIAN_POINT('Ctrl Pts',(7.28751437646116,-4.82697212643223,335.953118303829));
#68688=CARTESIAN_POINT('Ctrl Pts',(7.27975638474862,-4.79842484400952,336.087747520506));
#68689=CARTESIAN_POINT('Ctrl Pts',(7.27199839303609,-4.76430448091855,336.220895521984));
#68690=CARTESIAN_POINT('Ctrl Pts',(7.26423786358946,-4.730172956639,336.354087077803));
#68691=CARTESIAN_POINT('Ctrl Pts',(7.25647733414284,-4.69046481973589,336.485796077464));
#68692=CARTESIAN_POINT('Ctrl Pts',(7.24871680469622,-4.64534596146615,336.615532098347));
#68693=CARTESIAN_POINT('Ctrl Pts',(7.24094709317594,-4.60017371963766,336.745421619802));
#68694=CARTESIAN_POINT('Ctrl Pts',(7.23317738165566,-4.54957809758052,336.873333132058));
#68695=CARTESIAN_POINT('Ctrl Pts',(7.22540767013538,-4.49377363385272,336.998795034562));
#68696=CARTESIAN_POINT('Ctrl Pts',(7.21763315266209,-4.43793465228857,337.124334541493));
#68697=CARTESIAN_POINT('Ctrl Pts',(7.20985863518881,-4.37688058228527,337.247421071832));
#68698=CARTESIAN_POINT('Ctrl Pts',(7.20208411771551,-4.31087180155181,337.367607943281));
#68699=CARTESIAN_POINT('Ctrl Pts',(7.19429674930069,-4.24475391115534,337.487993478435));
#68700=CARTESIAN_POINT('Ctrl Pts',(7.18650938088584,-4.17366514813585,337.605469445913));
#68701=CARTESIAN_POINT('Ctrl Pts',(7.17872201247101,-4.09790953495292,337.71961771318));
#68702=CARTESIAN_POINT('Ctrl Pts',(7.1722596340402,-4.03504344019951,337.814344103535));
#68703=CARTESIAN_POINT('Ctrl Pts',(7.16579725560938,-3.96896432051202,337.906779326875));
#68704=CARTESIAN_POINT('Ctrl Pts',(7.15933487717857,-3.89986615034613,337.996702699949));
#68705=CARTESIAN_POINT('Ctrl Pts',(7.15156122621795,-3.81674736325525,338.104872303908));
#68706=CARTESIAN_POINT('Ctrl Pts',(7.14378757525728,-3.72899314005567,338.209752401944));
#68707=CARTESIAN_POINT('Ctrl Pts',(7.13601392429661,-3.63689323404313,338.310919912452));
#68708=CARTESIAN_POINT('Ctrl Pts',(7.12824984273351,-3.54490670340889,338.411962885321));
#68709=CARTESIAN_POINT('Ctrl Pts',(7.12048576117038,-3.4485853946733,338.509302077618));
#68710=CARTESIAN_POINT('Ctrl Pts',(7.11272167960729,-3.34826104067228,338.602545081747));
#68711=CARTESIAN_POINT('Ctrl Pts',(7.10496529775928,-3.24803617930738,338.695695615883));
#68712=CARTESIAN_POINT('Ctrl Pts',(7.09720891591133,-3.14381645743581,338.784757781369));
#68713=CARTESIAN_POINT('Ctrl Pts',(7.08945253406333,-3.0359721560843,338.869374126391));
#68714=CARTESIAN_POINT('Ctrl Pts',(7.08170198893485,-2.92820900815613,338.953926797152));
#68715=CARTESIAN_POINT('Ctrl Pts',(7.07395144380637,-2.81682701609293,339.034040066058));
#68716=CARTESIAN_POINT('Ctrl Pts',(7.06620089867789,-2.70223113714075,339.109395325832));
#68717=CARTESIAN_POINT('Ctrl Pts',(7.0584536295921,-2.58768369619975,339.184718734034));
#68718=CARTESIAN_POINT('Ctrl Pts',(7.05070636050632,-2.46992539625358,339.255287918658));
#68719=CARTESIAN_POINT('Ctrl Pts',(7.04295909142053,-2.3493917231837,339.320826494264));
#68720=CARTESIAN_POINT('Ctrl Pts',(7.03521343011243,-2.22888306426368,339.38635146876));
#68721=CARTESIAN_POINT('Ctrl Pts',(7.02746776880427,-2.10560052116608,339.446847724117));
#68722=CARTESIAN_POINT('Ctrl Pts',(7.01972210749616,-1.98000547773249,339.502084114124));
#68723=CARTESIAN_POINT('Ctrl Pts',(7.01197637554554,-1.85440928883823,339.557321007902));
#68724=CARTESIAN_POINT('Ctrl Pts',(7.00423064359498,-1.7265009154913,339.60729778324));
#68725=CARTESIAN_POINT('Ctrl Pts',(6.99648491164436,-1.5967627089283,339.651831028087));
#68726=CARTESIAN_POINT('Ctrl Pts',(6.98873743093975,-1.46699521136894,339.696374327206));
#68727=CARTESIAN_POINT('Ctrl Pts',(6.98098995023512,-1.33539742830905,339.735471523376));
#68728=CARTESIAN_POINT('Ctrl Pts',(6.9732424695305,-1.20246750549885,339.768988882428));
#68729=CARTESIAN_POINT('Ctrl Pts',(6.96548674509676,-1.06939613822188,339.802541905722));
#68730=CARTESIAN_POINT('Ctrl Pts',(6.95773102066302,-0.934990179439701,
339.830503135968));
#68731=CARTESIAN_POINT('Ctrl Pts',(6.94997529622927,-0.799759167171889,
339.852789747869));
#68732=CARTESIAN_POINT('Ctrl Pts',(6.94221541850505,-0.664455736952739,
339.875088294538));
#68733=CARTESIAN_POINT('Ctrl Pts',(6.93445554078086,-0.528326760827144,
339.891706120434));
#68734=CARTESIAN_POINT('Ctrl Pts',(6.92669566305665,-0.391886567790598,
339.902612362862));
#68735=CARTESIAN_POINT('Ctrl Pts',(6.91892334207123,-0.255227587677649,
339.913536093867));
#68736=CARTESIAN_POINT('Ctrl Pts',(6.91115102108579,-0.118256784361598,
339.918729924733));
#68737=CARTESIAN_POINT('Ctrl Pts',(6.90337870010038,0.0185109458667954,
339.918215164812));
#68738=CARTESIAN_POINT('Ctrl Pts',(6.89595141436849,0.149207170741441,339.917723256535));
#68739=CARTESIAN_POINT('Ctrl Pts',(6.88852412863661,0.279717674553717,339.912018754077));
#68740=CARTESIAN_POINT('Ctrl Pts',(6.88109684290473,0.409599680461112,339.901164266199));
#68741=CARTESIAN_POINT('Ctrl Pts',(6.87332050122199,0.545585677612053,339.889799656087));
#68742=CARTESIAN_POINT('Ctrl Pts',(6.86554415953925,0.681313005923244,339.872753288523));
#68743=CARTESIAN_POINT('Ctrl Pts',(6.85776781785651,0.816268807056172,339.850040030466));
#68744=CARTESIAN_POINT('Ctrl Pts',(6.85000105068764,0.951058445712975,339.827354737797));
#68745=CARTESIAN_POINT('Ctrl Pts',(6.84223428351876,1.08507806565111,339.799016501738));
#68746=CARTESIAN_POINT('Ctrl Pts',(6.83446751634989,1.21781790235197,339.765092089269));
#68747=CARTESIAN_POINT('Ctrl Pts',(6.82670845668871,1.3504260120047,339.731201342373));
#68748=CARTESIAN_POINT('Ctrl Pts',(6.81894939702748,1.48175648970576,339.691735547248));
#68749=CARTESIAN_POINT('Ctrl Pts',(6.8111903373663,1.61130811837897,339.646812801281));
#68750=CARTESIAN_POINT('Ctrl Pts',(6.80343712487902,1.74076211783737,339.601923908785));
#68751=CARTESIAN_POINT('Ctrl Pts',(6.79568391239175,1.86843956884725,339.551586378364));
#68752=CARTESIAN_POINT('Ctrl Pts',(6.78793069990448,1.9938531633102,339.495968485839));
#68753=CARTESIAN_POINT('Ctrl Pts',(6.78018078853269,2.11921335993852,339.440374273961));
#68754=CARTESIAN_POINT('Ctrl Pts',(6.77243087716089,2.24231126072714,339.37950432975));
#68755=CARTESIAN_POINT('Ctrl Pts',(6.7646809657891,2.36267854936551,339.313575446757));
#68756=CARTESIAN_POINT('Ctrl Pts',(6.75693267779888,2.48302062454926,339.247660373952));
#68757=CARTESIAN_POINT('Ctrl Pts',(6.74918438980871,2.60063288282723,339.1766886578));
#68758=CARTESIAN_POINT('Ctrl Pts',(6.74143610181849,2.71507103704166,339.100923350456));
#68759=CARTESIAN_POINT('Ctrl Pts',(6.73368776118936,2.82950996870531,339.025157528392));
#68760=CARTESIAN_POINT('Ctrl Pts',(6.72593942056018,2.94077442746838,338.944598265858));
#68761=CARTESIAN_POINT('Ctrl Pts',(6.71819107993105,3.04844891825089,338.859552079622));
#68762=CARTESIAN_POINT('Ctrl Pts',(6.71044101096481,3.15614742679748,338.774486923069));
#68763=CARTESIAN_POINT('Ctrl Pts',(6.70269094199856,3.26025406733491,338.684933093379));
#68764=CARTESIAN_POINT('Ctrl Pts',(6.69494087303232,3.36038656790733,338.591237276584));
#68765=CARTESIAN_POINT('Ctrl Pts',(6.68718260700293,3.4606249762381,338.497442359958));
#68766=CARTESIAN_POINT('Ctrl Pts',(6.67942434097348,3.5568805622272,338.399496972382));
#68767=CARTESIAN_POINT('Ctrl Pts',(6.67166607494408,3.64880769520589,338.29778493324));
#68768=CARTESIAN_POINT('Ctrl Pts',(6.66390367701195,3.74078378680122,338.19601872423));
#68769=CARTESIAN_POINT('Ctrl Pts',(6.65614127907988,3.82842658239426,338.09048216683));
#68770=CARTESIAN_POINT('Ctrl Pts',(6.64837888114775,3.91143154575164,337.981591240495));
#68771=CARTESIAN_POINT('Ctrl Pts',(6.64060410176749,3.99456890655333,337.872526627193));
#68772=CARTESIAN_POINT('Ctrl Pts',(6.63282932238728,4.07305342871677,337.760097273816));
#68773=CARTESIAN_POINT('Ctrl Pts',(6.62505454300702,4.14662413498238,337.644747879417));
#68774=CARTESIAN_POINT('Ctrl Pts',(6.61765596488162,4.21663494704854,337.534979940748));
#68775=CARTESIAN_POINT('Ctrl Pts',(6.6102573867562,4.28219618884176,337.422568170264));
#68776=CARTESIAN_POINT('Ctrl Pts',(6.6028588086308,4.34312291699588,337.307913861123));
#68777=CARTESIAN_POINT('Ctrl Pts',(6.59508121422942,4.40717081535613,337.187386011345));
#68778=CARTESIAN_POINT('Ctrl Pts',(6.58730361982803,4.46629835475321,337.064000567731));
#68779=CARTESIAN_POINT('Ctrl Pts',(6.57952602542665,4.52024059322292,336.938197111204));
#68780=CARTESIAN_POINT('Ctrl Pts',(6.57175797883564,4.57411661195453,336.812548091574));
#68781=CARTESIAN_POINT('Ctrl Pts',(6.5639899322446,4.6228198430109,336.684487320884));
#68782=CARTESIAN_POINT('Ctrl Pts',(6.5562218856536,4.66613067559802,336.554479842501));
#68783=CARTESIAN_POINT('Ctrl Pts',(6.54846152154273,4.70939867442934,336.424600939541));
#68784=CARTESIAN_POINT('Ctrl Pts',(6.54070115743189,4.74728476526471,336.292779528521));
#68785=CARTESIAN_POINT('Ctrl Pts',(6.53294079332102,4.77961713734269,336.159501221612));
#68786=CARTESIAN_POINT('Ctrl Pts',(6.52518625299873,4.81192524549478,336.02632293381));
#68787=CARTESIAN_POINT('Ctrl Pts',(6.51743171267646,4.83868783911139,335.89169030443));
#68788=CARTESIAN_POINT('Ctrl Pts',(6.50967717235417,4.8597828370889,335.756104383558));
#68789=CARTESIAN_POINT('Ctrl Pts',(6.5019259026434,4.88086893788613,335.620575648394));
#68790=CARTESIAN_POINT('Ctrl Pts',(6.4941746329326,4.89629213753075,335.484094806573));
#68791=CARTESIAN_POINT('Ctrl Pts',(6.48642336322183,4.90598143576346,335.347173176447));
#68792=CARTESIAN_POINT('Ctrl Pts',(6.47867369856857,4.91566872763059,335.210279898719));
#68793=CARTESIAN_POINT('Ctrl Pts',(6.47092403391527,4.91962445223797,335.072946403604));
#68794=CARTESIAN_POINT('Ctrl Pts',(6.46317436926199,4.91782951458132,334.935688818913));
#68795=CARTESIAN_POINT('Ctrl Pts',(6.45542463505456,4.9160345608149,334.798430002318));
#68796=CARTESIAN_POINT('Ctrl Pts',(6.44767490084714,4.90848884696551,334.661247488054));
#68797=CARTESIAN_POINT('Ctrl Pts',(6.43992516663971,4.89522540931375,334.52465669826));
#68798=CARTESIAN_POINT('Ctrl Pts',(6.43217368857847,4.88195898710851,334.388035172655));
#68799=CARTESIAN_POINT('Ctrl Pts',(6.42442221051726,4.8629723185987,334.252006025156));
#68800=CARTESIAN_POINT('Ctrl Pts',(6.41667073245603,4.83835019667313,334.117078465064));
#68801=CARTESIAN_POINT('Ctrl Pts',(6.40891104105662,4.81370198555369,333.982007937958));
#68802=CARTESIAN_POINT('Ctrl Pts',(6.40115134965721,4.78340646312433,333.848041714744));
#68803=CARTESIAN_POINT('Ctrl Pts',(6.3933916582578,4.74759947504644,333.71567827744));
#68804=CARTESIAN_POINT('Ctrl Pts',(6.38562782385426,4.71177336913359,333.583244169508));
#68805=CARTESIAN_POINT('Ctrl Pts',(6.37786398945076,4.67043005160834,333.452414924919));
#68806=CARTESIAN_POINT('Ctrl Pts',(6.37010015504723,4.62375464775931,333.323671863917));
#68807=CARTESIAN_POINT('Ctrl Pts',(6.36232393501272,4.57700478272297,333.194723419343));
#68808=CARTESIAN_POINT('Ctrl Pts',(6.35454771497819,4.52490598174406,333.067868170361));
#68809=CARTESIAN_POINT('Ctrl Pts',(6.34677149494368,4.46769108994829,332.943566342598));
#68810=CARTESIAN_POINT('Ctrl Pts',(6.33938792141474,4.41336516312913,332.825540916234));
#68811=CARTESIAN_POINT('Ctrl Pts',(6.33200434788581,4.35442727196074,332.709817616591));
#68812=CARTESIAN_POINT('Ctrl Pts',(6.32462077435687,4.29111327678704,332.596766780297));
#68813=CARTESIAN_POINT('Ctrl Pts',(6.31685531416248,4.22452461110345,332.477868828548));
#68814=CARTESIAN_POINT('Ctrl Pts',(6.3090898539681,4.15288382142553,332.36154993445));
#68815=CARTESIAN_POINT('Ctrl Pts',(6.30132439377371,4.07641570313481,332.248269984585));
#68816=CARTESIAN_POINT('Ctrl Pts',(6.2935685171197,4.00004195597996,332.135129836218));
#68817=CARTESIAN_POINT('Ctrl Pts',(6.28581264046562,3.91885295049355,332.02502149187));
#68818=CARTESIAN_POINT('Ctrl Pts',(6.27805676381161,3.83311947643843,331.918380597503));
#68819=CARTESIAN_POINT('Ctrl Pts',(6.27030859261078,3.74747117847623,331.811845650722));
#68820=CARTESIAN_POINT('Ctrl Pts',(6.26256042141,3.65728764039709,331.708771602173));
#68821=CARTESIAN_POINT('Ctrl Pts',(6.25481225020917,3.5628828680657,331.609565111826));
#68822=CARTESIAN_POINT('Ctrl Pts',(6.24706991314045,3.4685491795939,331.510433320884));
#68823=CARTESIAN_POINT('Ctrl Pts',(6.2393275760717,3.37000085219638,331.415163574706));
#68824=CARTESIAN_POINT('Ctrl Pts',(6.23158523900298,3.26759183428722,331.324129128084));
#68825=CARTESIAN_POINT('Ctrl Pts',(6.22384614567352,3.16522572178886,331.233132821369));
#68826=CARTESIAN_POINT('Ctrl Pts',(6.21610705234402,3.05900242779361,331.146368545235));
#68827=CARTESIAN_POINT('Ctrl Pts',(6.20836795901457,2.94931222402584,331.06417220045));
#68828=CARTESIAN_POINT('Ctrl Pts',(6.2006304528915,2.83964451656158,330.981992713267));
#68829=CARTESIAN_POINT('Ctrl Pts',(6.19289294676851,2.72651162694693,330.904379529035));
#68830=CARTESIAN_POINT('Ctrl Pts',(6.18515544064545,2.61033599307547,330.831627527949));
#68831=CARTESIAN_POINT('Ctrl Pts',(6.17741783588129,2.4941588781465,330.758874599389));
#68832=CARTESIAN_POINT('Ctrl Pts',(6.16968023111711,2.37493927381613,330.690983185531));
#68833=CARTESIAN_POINT('Ctrl Pts',(6.16194262635295,2.25312725560259,330.628203958033));
#68834=CARTESIAN_POINT('Ctrl Pts',(6.15420323738419,2.13128714890814,330.56541025435));
#68835=CARTESIAN_POINT('Ctrl Pts',(6.14646384841544,2.00685378717366,330.507731262158));
#68836=CARTESIAN_POINT('Ctrl Pts',(6.13872445944668,1.88030003422444,330.455370769381));
#68837=CARTESIAN_POINT('Ctrl Pts',(6.1309767254356,1.75360982393633,330.402953818591));
#68838=CARTESIAN_POINT('Ctrl Pts',(6.12322899142452,1.62479501807467,330.355866972769));
#68839=CARTESIAN_POINT('Ctrl Pts',(6.11548125741345,1.49434708877615,330.314265282715));
#68840=CARTESIAN_POINT('Ctrl Pts',(6.10772932783854,1.36382851913112,330.272641064455));
#68841=CARTESIAN_POINT('Ctrl Pts',(6.09997739826369,1.2316754418383,330.236508023425));
#68842=CARTESIAN_POINT('Ctrl Pts',(6.09222546868878,1.09839153265352,330.205970473235));
#68843=CARTESIAN_POINT('Ctrl Pts',(6.08446094315674,0.964891053079382,330.175383303183));
#68844=CARTESIAN_POINT('Ctrl Pts',(6.07669641762463,0.830256455393671,330.150409863777));
#68845=CARTESIAN_POINT('Ctrl Pts',(6.06893189209259,0.694999476123359,330.131102918454));
#68846=CARTESIAN_POINT('Ctrl Pts',(6.06141550808936,0.564065088552856,330.112412991507));
#68847=CARTESIAN_POINT('Ctrl Pts',(6.0538991240861,0.432547813631449,330.099032887664));
#68848=CARTESIAN_POINT('Ctrl Pts',(6.04638274008286,0.300911661534685,330.090963920029));
#68849=CARTESIAN_POINT('Ctrl Pts',(6.03859686493552,0.164555849396764,330.082605649012));
#68850=CARTESIAN_POINT('Ctrl Pts',(6.03081098978817,0.0276383429979844,
330.079919834404));
#68851=CARTESIAN_POINT('Ctrl Pts',(6.02302511464083,-0.109330180294248,
330.082965327133));
#68852=CARTESIAN_POINT('Ctrl Pts',(6.0152488453941,-0.246129717313841,330.086007062456));
#68853=CARTESIAN_POINT('Ctrl Pts',(6.00747257614737,-0.382979760028109,
330.094766026414));
#68854=CARTESIAN_POINT('Ctrl Pts',(5.99969630690063,-0.519365263713141,
330.109249261581));
#68855=CARTESIAN_POINT('Ctrl Pts',(5.99192778607104,-0.655614870383523,
330.123718065387));
#68856=CARTESIAN_POINT('Ctrl Pts',(5.98415926524146,-0.791400474143886,
330.143899748102));
#68857=CARTESIAN_POINT('Ctrl Pts',(5.97639074441187,-0.926208128716363,
330.169749326919));
#68858=CARTESIAN_POINT('Ctrl Pts',(5.96862812115544,-1.06091344231262,330.195579281693));
#68859=CARTESIAN_POINT('Ctrl Pts',(5.96086549789901,-1.19464190332912,330.22706849442));
#68860=CARTESIAN_POINT('Ctrl Pts',(5.95310287464258,-1.32688612205344,330.264120326528));
#68861=CARTESIAN_POINT('Ctrl Pts',(5.94534366171854,-1.45907224228106,330.301155880755));
#68862=CARTESIAN_POINT('Ctrl Pts',(5.93758444879453,-1.58977504287365,330.343749088023));
#68863=CARTESIAN_POINT('Ctrl Pts',(5.92982523587048,-1.7184989556453,330.391752567196));
#68864=CARTESIAN_POINT('Ctrl Pts',(5.92206771428337,-1.8471948094488,330.439745582671));
#68865=CARTESIAN_POINT('Ctrl Pts',(5.91431019269621,-1.97391226858973,330.493146387989));
#68866=CARTESIAN_POINT('Ctrl Pts',(5.9065526711091,-2.09817287370277,330.55175836374));
#68867=CARTESIAN_POINT('Ctrl Pts',(5.89879517343114,-2.22243309583706,330.610370158845));
#68868=CARTESIAN_POINT('Ctrl Pts',(5.89103767575322,-2.34423612646736,330.67419292631));
#68869=CARTESIAN_POINT('Ctrl Pts',(5.88328017807527,-2.46312571868049,330.742982880411));
#68870=CARTESIAN_POINT('Ctrl Pts',(5.8755210372566,-2.58204049328334,330.811787405135));
#68871=CARTESIAN_POINT('Ctrl Pts',(5.8677618964379,-2.69804026419989,330.885561014991));
#68872=CARTESIAN_POINT('Ctrl Pts',(5.86000275561923,-2.81069584596198,330.96401537119));
#68873=CARTESIAN_POINT('Ctrl Pts',(5.85223560277196,-2.92346775500368,331.042550738749));
#68874=CARTESIAN_POINT('Ctrl Pts',(5.84446844992471,-3.03288825638894,331.125776284726));
#68875=CARTESIAN_POINT('Ctrl Pts',(5.83670129707744,-3.13855905018823,331.213361629231));
#68876=CARTESIAN_POINT('Ctrl Pts',(5.82893009938131,-3.24428487346845,331.300992584977));
#68877=CARTESIAN_POINT('Ctrl Pts',(5.82115890168517,-3.34625680853045,331.392987602795));
#68878=CARTESIAN_POINT('Ctrl Pts',(5.81338770398904,-3.44411254127841,331.488978515374));
#68879=CARTESIAN_POINT('Ctrl Pts',(5.80560436101053,-3.5421212086901,331.585119448166));
#68880=CARTESIAN_POINT('Ctrl Pts',(5.79782101803203,-3.63600055173004,331.685268470824));
#68881=CARTESIAN_POINT('Ctrl Pts',(5.79003767505353,-3.7254271888263,331.789022684095));
#68882=CARTESIAN_POINT('Ctrl Pts',(5.78274001863869,-3.80927353526954,331.886302554986));
#68883=CARTESIAN_POINT('Ctrl Pts',(5.77544236222388,-3.88920577385065,331.986751200925));
#68884=CARTESIAN_POINT('Ctrl Pts',(5.76814470580905,-3.96499237429082,332.090013997574));
#68885=CARTESIAN_POINT('Ctrl Pts',(5.76033139000508,-4.04613412847658,332.200573442298));
#68886=CARTESIAN_POINT('Ctrl Pts',(5.75251807420117,-4.12277500424751,332.314702062708));
#68887=CARTESIAN_POINT('Ctrl Pts',(5.74470475839726,-4.19458675120634,332.431999795735));
#68888=CARTESIAN_POINT('Ctrl Pts',(5.73690099457361,-4.26631070645083,332.549154129256));
#68889=CARTESIAN_POINT('Ctrl Pts',(5.72909723074999,-4.33321707948485,332.669469541798));
#68890=CARTESIAN_POINT('Ctrl Pts',(5.72129346692634,-4.39501868564208,332.792514141527));
#68891=CARTESIAN_POINT('Ctrl Pts',(5.71349761094548,-4.45675766594377,332.915434055608));
#68892=CARTESIAN_POINT('Ctrl Pts',(5.70570175496459,-4.51340200123606,333.041077311382));
#68893=CARTESIAN_POINT('Ctrl Pts',(5.69790589898372,-4.56470872838734,333.16898462937));
#68894=CARTESIAN_POINT('Ctrl Pts',(5.69011631244605,-4.61597419456453,333.296789084033));
#68895=CARTESIAN_POINT('Ctrl Pts',(5.68232672590839,-4.661910453602,333.426853620556));
#68896=CARTESIAN_POINT('Ctrl Pts',(5.67453713937073,-4.70232142528769,333.558696327702));
#68897=CARTESIAN_POINT('Ctrl Pts',(5.66675225035573,-4.74270802707204,333.690459526891));
#68898=CARTESIAN_POINT('Ctrl Pts',(5.65896736134076,-4.77757586349578,333.823998393796));
#68899=CARTESIAN_POINT('Ctrl Pts',(5.65118247232576,-4.80677787629,333.958813412251));
#68900=CARTESIAN_POINT('Ctrl Pts',(5.64340035908543,-4.83596947683462,334.093580361155));
#68901=CARTESIAN_POINT('Ctrl Pts',(5.63561824584508,-4.85949919536628,334.229622179123));
#68902=CARTESIAN_POINT('Ctrl Pts',(5.62783613260476,-4.87727056797979,334.366426903019));
#68903=CARTESIAN_POINT('Ctrl Pts',(5.6200540689251,-4.89504182741568,334.503230755669));
#68904=CARTESIAN_POINT('Ctrl Pts',(5.6122720052455,-4.9070547585848,334.640797123079));
#68905=CARTESIAN_POINT('Ctrl Pts',(5.60448994156584,-4.91326450350974,334.778606727629));
#68906=CARTESIAN_POINT('Ctrl Pts',(5.60026575321351,-4.91663522023254,334.853411271815));
#68907=CARTESIAN_POINT('Ctrl Pts',(5.59604156486116,-4.91829696519244,334.928287391275));
#68908=CARTESIAN_POINT('Ctrl Pts',(5.59181737650883,-4.91824899013982,335.003151743738));
#68909=CARTESIAN_POINT('Origin',(186.231676812499,0.,335.));
#68910=CARTESIAN_POINT('',(186.231676812499,-7.,335.));
#68911=CARTESIAN_POINT('Origin',(186.231676812499,0.,335.));
#68912=CARTESIAN_POINT('',(186.231676812499,5.77350269189626,335.));
#68913=CARTESIAN_POINT('',(186.231676812499,2.88675134594813,340.));
#68914=CARTESIAN_POINT('',(186.231676812499,5.05181485540923,336.25));
#68915=CARTESIAN_POINT('',(186.231676812499,2.88675134594813,330.));
#68916=CARTESIAN_POINT('',(186.231676812499,3.60843918243516,331.25));
#68917=CARTESIAN_POINT('',(186.231676812499,-2.88675134594813,330.));
#68918=CARTESIAN_POINT('',(186.231676812499,-1.44337567297406,330.));
#68919=CARTESIAN_POINT('',(186.231676812499,-5.77350269189625,335.));
#68920=CARTESIAN_POINT('',(186.231676812499,-5.05181485540922,333.75));
#68921=CARTESIAN_POINT('',(186.231676812499,-2.88675134594811,340.));
#68922=CARTESIAN_POINT('',(186.231676812499,-3.60843918243515,338.75));
#68923=CARTESIAN_POINT('',(186.231676812499,1.44337567297406,340.));
#68924=CARTESIAN_POINT('Origin',(185.231676812499,0.,335.));
#68925=CARTESIAN_POINT('',(185.231676812499,-7.,335.));
#68926=CARTESIAN_POINT('',(185.231676812499,-7.,335.));
#68927=CARTESIAN_POINT('Origin',(185.231676812499,0.,335.));
#68928=CARTESIAN_POINT('Origin',(185.231676812499,-5.77350269189625,335.));
#68929=CARTESIAN_POINT('',(205.231676812499,-2.88675134594813,330.));
#68930=CARTESIAN_POINT('',(185.231676812499,-2.88675134594813,330.));
#68931=CARTESIAN_POINT('',(205.231676812499,-5.77350269189625,335.));
#68932=CARTESIAN_POINT('',(205.231676812499,-5.77350269189625,335.));
#68933=CARTESIAN_POINT('',(185.231676812499,-5.77350269189625,335.));
#68934=CARTESIAN_POINT('Origin',(185.231676812499,-2.88675134594813,330.));
#68935=CARTESIAN_POINT('',(205.231676812499,2.88675134594813,330.));
#68936=CARTESIAN_POINT('',(185.231676812499,2.88675134594813,330.));
#68937=CARTESIAN_POINT('',(205.231676812499,-2.88675134594813,330.));
#68938=CARTESIAN_POINT('Origin',(185.231676812499,2.88675134594813,330.));
#68939=CARTESIAN_POINT('',(205.231676812499,5.77350269189626,335.));
#68940=CARTESIAN_POINT('',(185.231676812499,5.77350269189626,335.));
#68941=CARTESIAN_POINT('',(205.231676812499,2.88675134594813,330.));
#68942=CARTESIAN_POINT('Origin',(185.231676812499,4.44089209850063E-15,
335.));
#68943=CARTESIAN_POINT('',(185.23167683184,-3.96013600436147,338.142060500916));
#68944=CARTESIAN_POINT('Ctrl Pts',(185.231676812499,-3.96013605566283,338.142060549271));
#68945=CARTESIAN_POINT('Ctrl Pts',(185.231676812499,-4.28438313788062,337.798053387465));
#68946=CARTESIAN_POINT('Ctrl Pts',(185.231676812499,-4.5597175012955,337.407746480001));
#68947=CARTESIAN_POINT('Ctrl Pts',(185.231676812499,-5.00660837949084,336.559057380709));
#68948=CARTESIAN_POINT('Ctrl Pts',(185.231676812499,-5.17583108149262,336.097536688629));
#68949=CARTESIAN_POINT('Ctrl Pts',(185.231676812499,-5.43533327152918,334.920836850492));
#68950=CARTESIAN_POINT('Ctrl Pts',(185.231676812499,-5.44158388072912,334.250043530421));
#68951=CARTESIAN_POINT('Ctrl Pts',(185.231676812499,-5.19996495846416,332.894580477494));
#68952=CARTESIAN_POINT('Ctrl Pts',(185.231676812499,-4.93922833436616,332.223849290227));
#68953=CARTESIAN_POINT('Ctrl Pts',(185.231676812499,-4.3237022218484,331.228008604537));
#68954=CARTESIAN_POINT('Ctrl Pts',(185.231676812499,-4.03283623373639,330.863982759591));
#68955=CARTESIAN_POINT('Ctrl Pts',(185.231676812499,-3.36666521490454,330.20750410331));
#68956=CARTESIAN_POINT('Ctrl Pts',(185.231676812499,-2.99060132980376,329.917370541692));
#68957=CARTESIAN_POINT('Ctrl Pts',(185.231676812499,-2.58391981634258,329.677285566066));
#68958=CARTESIAN_POINT('',(185.229482559938,5.39695405107274,334.345551452481));
#68959=CARTESIAN_POINT('Ctrl Pts',(185.227994231758,2.5854165783574,329.675696584773));
#68960=CARTESIAN_POINT('Ctrl Pts',(185.227640459499,2.7081737407366,329.747941861091));
#68961=CARTESIAN_POINT('Ctrl Pts',(185.227524853352,2.82806177680362,329.8243971901));
#68962=CARTESIAN_POINT('Ctrl Pts',(185.227590200135,2.94476028939518,329.90515414262));
#68963=CARTESIAN_POINT('Ctrl Pts',(185.227662105192,3.07317079076938,329.99401595013));
#68964=CARTESIAN_POINT('Ctrl Pts',(185.227953107064,3.19772021473749,330.088086613307));
#68965=CARTESIAN_POINT('Ctrl Pts',(185.228386979994,3.31819273430149,330.187071053314));
#68966=CARTESIAN_POINT('Ctrl Pts',(185.228821913669,3.43895978855643,330.286297493335));
#68967=CARTESIAN_POINT('Ctrl Pts',(185.229400417846,3.55562982264465,330.390462569785));
#68968=CARTESIAN_POINT('Ctrl Pts',(185.230045706324,3.66793313993279,330.499263559958));
#68969=CARTESIAN_POINT('Ctrl Pts',(185.230688110766,3.77973453152617,330.60757827765));
#68970=CARTESIAN_POINT('Ctrl Pts',(185.231396703875,3.88720789030099,330.720488276194));
#68971=CARTESIAN_POINT('Ctrl Pts',(185.232095724413,3.99003858553928,330.837678118006));
#68972=CARTESIAN_POINT('Ctrl Pts',(185.232737549218,4.08445539794597,330.945279173165));
#68973=CARTESIAN_POINT('Ctrl Pts',(185.233371303873,4.17495751476312,331.056488543143));
#68974=CARTESIAN_POINT('Ctrl Pts',(185.233938343949,4.26126815979221,331.171042131527));
#68975=CARTESIAN_POINT('Ctrl Pts',(185.234525681538,4.35066834219649,331.289696229098));
#68976=CARTESIAN_POINT('Ctrl Pts',(185.234997494895,4.43522375791577,331.411591120723));
#68977=CARTESIAN_POINT('Ctrl Pts',(185.23535434099,4.51484630737464,331.536408496964));
#68978=CARTESIAN_POINT('Ctrl Pts',(185.235715534686,4.59543893075985,331.662746574099));
#68979=CARTESIAN_POINT('Ctrl Pts',(185.23595894267,4.67097812182971,331.792079505726));
#68980=CARTESIAN_POINT('Ctrl Pts',(185.236085142519,4.7413275791168,331.924105489045));
#68981=CARTESIAN_POINT('Ctrl Pts',(185.236210806957,4.81137857461677,332.05557134422));
#68982=CARTESIAN_POINT('Ctrl Pts',(185.236220255677,4.87628401583103,332.189708219156));
#68983=CARTESIAN_POINT('Ctrl Pts',(185.236114058936,4.93586070137055,332.326234669537));
#68984=CARTESIAN_POINT('Ctrl Pts',(185.236010030404,4.99422101533023,332.459973672234));
#68985=CARTESIAN_POINT('Ctrl Pts',(185.235795030449,5.0474680260653,332.596006376573));
#68986=CARTESIAN_POINT('Ctrl Pts',(185.235469595109,5.09538063730756,332.734073214484));
#68987=CARTESIAN_POINT('Ctrl Pts',(185.235167173811,5.13990497844604,332.862376281915));
#68988=CARTESIAN_POINT('Ctrl Pts',(185.234769384316,5.17982239323938,332.992436422879));
#68989=CARTESIAN_POINT('Ctrl Pts',(185.234276656793,5.21491522649548,333.124041555105));
#68990=CARTESIAN_POINT('Ctrl Pts',(185.233707355273,5.25546178082372,333.276099230379));
#68991=CARTESIAN_POINT('Ctrl Pts',(185.233047946604,5.28946248209387,333.429600643541));
#68992=CARTESIAN_POINT('Ctrl Pts',(185.232384613167,5.3168113587751,333.584078469419));
#68993=CARTESIAN_POINT('Ctrl Pts',(185.231733768864,5.343645315285,333.735647812088));
#68994=CARTESIAN_POINT('Ctrl Pts',(185.23107914619,5.36407628133255,333.888157544675));
#68995=CARTESIAN_POINT('Ctrl Pts',(185.230502150722,5.37797927517833,334.041209013612));
#68996=CARTESIAN_POINT('Ctrl Pts',(185.230120463025,5.38717623078736,334.142453938362));
#68997=CARTESIAN_POINT('Ctrl Pts',(185.229772744539,5.3935160662643,334.243936791883));
#68998=CARTESIAN_POINT('Ctrl Pts',(185.229482559938,5.39695405107274,334.345551452481));
#68999=CARTESIAN_POINT('',(185.231676812499,5.18549872251091,336.021916810612));
#69000=CARTESIAN_POINT('Ctrl Pts',(185.231676812499,5.4007694079033,334.346099854067));
#69001=CARTESIAN_POINT('Ctrl Pts',(185.231676812499,5.40584147874406,334.477371134359));
#69002=CARTESIAN_POINT('Ctrl Pts',(185.231676812499,5.40590729260707,334.608862633821));
#69003=CARTESIAN_POINT('Ctrl Pts',(185.231676812499,5.40076593664994,334.740348989421));
#69004=CARTESIAN_POINT('Ctrl Pts',(185.231676812499,5.39466110985939,334.89647539517));
#69005=CARTESIAN_POINT('Ctrl Pts',(185.231676812499,5.38121472107825,335.052595876397));
#69006=CARTESIAN_POINT('Ctrl Pts',(185.231676812499,5.36057609261863,335.208219833612));
#69007=CARTESIAN_POINT('Ctrl Pts',(185.231676812499,5.3582462039911,335.225788175849));
#69008=CARTESIAN_POINT('Ctrl Pts',(185.231676812499,5.35582407669609,335.24335377265));
#69009=CARTESIAN_POINT('Ctrl Pts',(185.231676812499,5.35331226641627,335.260899704573));
#69010=CARTESIAN_POINT('Ctrl Pts',(185.231676812499,5.3317196398837,335.411732256789));
#69011=CARTESIAN_POINT('Ctrl Pts',(185.231676812499,5.30346550590915,335.561410147836));
#69012=CARTESIAN_POINT('Ctrl Pts',(185.231676812499,5.26880078272557,335.709514464873));
#69013=CARTESIAN_POINT('Ctrl Pts',(185.231676812499,5.24423048589748,335.814490552864));
#69014=CARTESIAN_POINT('Ctrl Pts',(185.231676812499,5.21643836800517,335.918675990125));
#69015=CARTESIAN_POINT('Ctrl Pts',(185.231676812499,5.18549872286584,336.021916809428));
#69016=CARTESIAN_POINT('Ctrl Pts',(185.231676812499,5.18549872251113,336.021916810612));
#69017=CARTESIAN_POINT('Ctrl Pts',(185.231676812499,5.05958569114637,336.442069157206));
#69018=CARTESIAN_POINT('Ctrl Pts',(185.231676812498,4.88129210995362,336.847360621326));
#69019=CARTESIAN_POINT('Ctrl Pts',(185.231676812498,4.4356744775517,337.590470320891));
#69020=CARTESIAN_POINT('Ctrl Pts',(185.231676812498,4.17082293995955,337.929261543294));
#69021=CARTESIAN_POINT('Ctrl Pts',(185.231676812498,3.56527418889084,338.529985313398));
#69022=CARTESIAN_POINT('Ctrl Pts',(185.231676812499,3.22591379223974,338.791088436061));
#69023=CARTESIAN_POINT('Ctrl Pts',(185.231676812499,2.8570646345848,339.00329423554));
#69024=CARTESIAN_POINT('Ctrl Pts',(185.231676812499,-2.86416480220691,339.00656505702));
#69025=CARTESIAN_POINT('Ctrl Pts',(185.231676812499,-2.96718909511977,338.948123090184));
#69026=CARTESIAN_POINT('Ctrl Pts',(185.231676812499,-3.06770027579107,338.885880925931));
#69027=CARTESIAN_POINT('Ctrl Pts',(185.231676812499,-3.16545727640773,338.819900221475));
#69028=CARTESIAN_POINT('Ctrl Pts',(185.231676812499,-3.28283399218438,338.740677267162));
#69029=CARTESIAN_POINT('Ctrl Pts',(185.231676812499,-3.39624147032995,338.656066420927));
#69030=CARTESIAN_POINT('Ctrl Pts',(185.231676812499,-3.5055969172483,338.566518159339));
#69031=CARTESIAN_POINT('Ctrl Pts',(185.231676812499,-3.61495236416665,338.476969897751));
#69032=CARTESIAN_POINT('Ctrl Pts',(185.231676812499,-3.7202561302643,338.38248371036));
#69033=CARTESIAN_POINT('Ctrl Pts',(185.231676812499,-3.82140495863234,338.283461318034));
#69034=CARTESIAN_POINT('Ctrl Pts',(185.231676812499,-3.86855595085661,338.237301573764));
#69035=CARTESIAN_POINT('Ctrl Pts',(185.231676812499,-3.91480375207395,338.190155468001));
#69036=CARTESIAN_POINT('Ctrl Pts',(185.231676812499,-3.96013605261152,338.142060552508));
#69037=CARTESIAN_POINT('Origin',(185.231676812499,5.77350269189626,335.));
#69038=CARTESIAN_POINT('',(205.231676812499,2.88675134594813,340.));
#69039=CARTESIAN_POINT('',(185.231676812499,2.88675134594813,340.));
#69040=CARTESIAN_POINT('',(205.231676812499,5.77350269189626,335.));
#69041=CARTESIAN_POINT('Origin',(185.231676812499,-2.88675134594811,340.));
#69042=CARTESIAN_POINT('',(205.231676812499,-2.88675134594811,340.));
#69043=CARTESIAN_POINT('',(205.231676812499,-2.88675134594811,340.));
#69044=CARTESIAN_POINT('',(185.231676812499,-2.88675134594811,340.));
#69045=CARTESIAN_POINT('Origin',(185.231676812499,2.88675134594813,340.));
#69046=CARTESIAN_POINT('',(205.231676812499,2.88675134594813,340.));
#69047=CARTESIAN_POINT('Origin',(205.231676812499,4.44089209850063E-15,
335.));
#69048=CARTESIAN_POINT('Ctrl Pts',(185.811080378289,-2.14557563496124,330.580037935284));
#69049=CARTESIAN_POINT('Ctrl Pts',(185.764705644279,-2.88151516997222,330.937283427965));
#69050=CARTESIAN_POINT('Ctrl Pts',(185.671957904555,-4.15942683785613,332.026471253785));
#69051=CARTESIAN_POINT('Ctrl Pts',(185.486464153408,-5.4171251388755,335.17484951642));
#69052=CARTESIAN_POINT('Ctrl Pts',(185.254599124846,-3.7104720235285,339.469931545235));
#69053=CARTESIAN_POINT('Ctrl Pts',(184.976361090572,1.75984649753305,340.540119552943));
#69054=CARTESIAN_POINT('Ctrl Pts',(184.698123056299,5.60655848723213,336.517695725471));
#69055=CARTESIAN_POINT('Ctrl Pts',(184.419885022024,4.31271335213631,331.106893305836));
#69056=CARTESIAN_POINT('Ctrl Pts',(184.141646987751,-0.941219558116164,
329.266428853344));
#69057=CARTESIAN_POINT('Ctrl Pts',(183.863408953476,-5.33015269272146,332.688798752324));
#69058=CARTESIAN_POINT('Ctrl Pts',(183.585170919203,-4.82834868771287,338.231477647666));
#69059=CARTESIAN_POINT('Ctrl Pts',(183.306932884928,0.104711979366552,340.809019443882));
#69060=CARTESIAN_POINT('Ctrl Pts',(183.028694850655,4.94149341094068,338.055528588394));
#69061=CARTESIAN_POINT('Ctrl Pts',(182.750456816381,5.24363809821535,332.498120236651));
#69062=CARTESIAN_POINT('Ctrl Pts',(182.472218782107,0.733721161916883,329.236599179529));
#69063=CARTESIAN_POINT('Ctrl Pts',(182.193980747833,-4.44949313718591,331.264092910913));
#69064=CARTESIAN_POINT('Ctrl Pts',(181.915742713559,-5.54948793815025,336.719959177412));
#69065=CARTESIAN_POINT('Ctrl Pts',(181.637504679285,-1.556791794289,340.59745184479));
#69066=CARTESIAN_POINT('Ctrl Pts',(181.359266645011,3.86454508368571,339.338241573188));
#69067=CARTESIAN_POINT('Ctrl Pts',(181.081028610737,5.73944815949048,334.097893160242));
#69068=CARTESIAN_POINT('Ctrl Pts',(180.802790576463,2.34734321862604,329.685393757349));
#69069=CARTESIAN_POINT('Ctrl Pts',(180.524552542189,-3.19888333564474,330.150030653944));
#69070=CARTESIAN_POINT('Ctrl Pts',(180.246314507915,-5.80954219213952,335.065412519364));
#69071=CARTESIAN_POINT('Ctrl Pts',(179.968076473641,-3.08886975606896,339.920766447875));
#69072=CARTESIAN_POINT('Ctrl Pts',(179.689838439367,2.46641277265436,340.260405549321));
#69073=CARTESIAN_POINT('Ctrl Pts',(179.411600405093,5.75830475221954,335.772648168347));
#69074=CARTESIAN_POINT('Ctrl Pts',(179.13336237082,3.76588542763037,330.575842942801));
#69075=CARTESIAN_POINT('Ctrl Pts',(178.855124336545,-1.68243135602239,329.439021361301));
#69076=CARTESIAN_POINT('Ctrl Pts',(178.576886302272,-5.58680572404651,333.405427789685));
#69077=CARTESIAN_POINT('Ctrl Pts',(178.298648267998,-4.36425093644542,338.835149603303));
#69078=CARTESIAN_POINT('Ctrl Pts',(178.020410233724,0.863312517288815,340.745411230739));
#69079=CARTESIAN_POINT('Ctrl Pts',(177.74217219945,5.2986268174406,337.383193774887));
#69080=CARTESIAN_POINT('Ctrl Pts',(177.463934165176,4.87146949426853,331.833954567158));
#69081=CARTESIAN_POINT('Ctrl Pts',(177.185696130902,-0.0261634807241003,
329.190148522684));
#69082=CARTESIAN_POINT('Ctrl Pts',(176.907458096628,-4.89978661578628,331.877957425521));
#69083=CARTESIAN_POINT('Ctrl Pts',(176.629220062354,-5.27694789418978,337.430818717767));
#69084=CARTESIAN_POINT('Ctrl Pts',(176.35098202808,-0.811531977762798,340.752953551501));
#69085=CARTESIAN_POINT('Ctrl Pts',(176.072743993806,4.39861485648817,338.795687824499));
#69086=CARTESIAN_POINT('Ctrl Pts',(175.794505959532,5.57221776037641,333.355175405204));
#69087=CARTESIAN_POINT('Ctrl Pts',(175.516267925258,1.63227867137313,329.424094238988));
#69088=CARTESIAN_POINT('Ctrl Pts',(175.238029890984,-3.80557846195905,330.609939489414));
#69089=CARTESIAN_POINT('Ctrl Pts',(174.95979185671,-5.7511124109956,335.824478473221));
#69090=CARTESIAN_POINT('Ctrl Pts',(174.681553822436,-2.41893538674252,340.282405731434));
#69091=CARTESIAN_POINT('Ctrl Pts',(174.403315788163,3.1330629384969,339.892747218091));
#69092=CARTESIAN_POINT('Ctrl Pts',(174.125077753888,5.80989564901061,335.013086799536));
#69093=CARTESIAN_POINT('Ctrl Pts',(173.846839719615,3.15507287634666,330.121416818209));
#69094=CARTESIAN_POINT('Ctrl Pts',(173.56860168534,-2.39511370614138,329.706750615041));
#69095=CARTESIAN_POINT('Ctrl Pts',(173.290363651067,-5.74733979232378,334.149621244218));
#69096=CARTESIAN_POINT('Ctrl Pts',(173.012125616793,-3.82531698168697,339.372871906006));
#69097=CARTESIAN_POINT('Ctrl Pts',(172.733887582519,1.60714276145788,340.583202563136));
#69098=CARTESIAN_POINT('Ctrl Pts',(172.455649548245,5.56475131380112,336.669910636011));
#69099=CARTESIAN_POINT('Ctrl Pts',(172.177411513971,4.41566972106383,331.22416636606));
#69100=CARTESIAN_POINT('Ctrl Pts',(171.899173479697,-0.78560679951547,329.243448890762));
#69101=CARTESIAN_POINT('Ctrl Pts',(171.620935445424,-5.26594355571678,332.545433401856));
#69102=CARTESIAN_POINT('Ctrl Pts',(171.342697411149,-4.91380163603628,338.099937450725));
#69103=CARTESIAN_POINT('Ctrl Pts',(171.064459376875,-0.0523364825585829,
340.809674656063));
#69104=CARTESIAN_POINT('Ctrl Pts',(170.786221342601,4.85715708847794,338.187959180191));
#69105=CARTESIAN_POINT('Ctrl Pts',(170.507983308327,5.30930929093936,332.640700618857));
#69106=CARTESIAN_POINT('Ctrl Pts',(170.229745274054,0.88918672238244,329.258536276397));
#69107=CARTESIAN_POINT('Ctrl Pts',(169.951507239779,-4.34692937693034,331.145228449221));
#69108=CARTESIAN_POINT('Ctrl Pts',(169.673269205506,-5.59393254760659,336.569387577861));
#69109=CARTESIAN_POINT('Ctrl Pts',(169.395031171231,-1.70746638565333,340.553342890419));
#69110=CARTESIAN_POINT('Ctrl Pts',(169.116793136958,3.74591647625145,339.441077399649));
#69111=CARTESIAN_POINT('Ctrl Pts',(168.838555102684,5.76172707753682,334.253300729414));
#69112=CARTESIAN_POINT('Ctrl Pts',(168.56031706841,2.49008578271897,329.750758958534));
#69113=CARTESIAN_POINT('Ctrl Pts',(168.282079034136,-3.06667048129415,330.065368212736));
#69114=CARTESIAN_POINT('Ctrl Pts',(168.003840999862,-5.80918850860578,334.908416223065));
#69115=CARTESIAN_POINT('Ctrl Pts',(167.725602965588,-3.22069998505172,339.835509313713));
#69116=CARTESIAN_POINT('Ctrl Pts',(167.447364931314,2.32337737733045,340.325126879166));
#69117=CARTESIAN_POINT('Ctrl Pts',(167.16912689704,5.73532561353033,335.927954106353));
#69118=CARTESIAN_POINT('Ctrl Pts',(166.890888862766,3.88405018746073,330.67921154672));
#69119=CARTESIAN_POINT('Ctrl Pts',(166.612650828492,-1.5315607671548,329.395592775929));
#69120=CARTESIAN_POINT('Ctrl Pts',(166.334412794218,-5.54168101155223,333.255055793753));
#69121=CARTESIAN_POINT('Ctrl Pts',(166.056174759944,-4.46628238672583,338.715828354316));
#69122=CARTESIAN_POINT('Ctrl Pts',(165.77793672567,0.707757662178901,340.76664007966));
#69123=CARTESIAN_POINT('Ctrl Pts',(165.499698691397,5.23229895098799,337.525491319368));
#69124=CARTESIAN_POINT('Ctrl Pts',(165.221460657123,4.95523672108138,331.966736451483));
#69125=CARTESIAN_POINT('Ctrl Pts',(164.943222622848,0.130826891412531,329.191562771176));
#69126=CARTESIAN_POINT('Ctrl Pts',(164.664984588575,-4.81364084550388,331.746706203367));
#69127=CARTESIAN_POINT('Ctrl Pts',(164.3867465543,-5.34070142772378,337.287349334192));
#69128=CARTESIAN_POINT('Ctrl Pts',(164.108508520027,-0.96667913834544,340.728925742249));
#69129=CARTESIAN_POINT('Ctrl Pts',(163.830270485753,4.29445032813183,338.913151555451));
#69130=CARTESIAN_POINT('Ctrl Pts',(163.552032451479,5.61462611446546,333.506335944236));
#69131=CARTESIAN_POINT('Ctrl Pts',(163.273794417205,1.78234238729975,329.470233790553));
#69132=CARTESIAN_POINT('Ctrl Pts',(162.995556382931,-3.68557064136043,330.508716468062));
#69133=CARTESIAN_POINT('Ctrl Pts',(162.717318348657,-5.77128989137762,335.668783751595));
#69134=CARTESIAN_POINT('Ctrl Pts',(162.439080314383,-2.56078159217679,340.215118057522));
#69135=CARTESIAN_POINT('Ctrl Pts',(162.160842280109,2.99971817709032,339.975615497076));
#69136=CARTESIAN_POINT('Ctrl Pts',(161.882604245835,5.80742085100939,335.17006403493));
#69137=CARTESIAN_POINT('Ctrl Pts',(161.604366211561,3.28573912734839,330.208447318068));
#69138=CARTESIAN_POINT('Ctrl Pts',(161.326128177287,-2.2512168960502,329.643967774215));
#69139=CARTESIAN_POINT('Ctrl Pts',(161.047890143014,-5.72226440185046,333.994639949058));
#69140=CARTESIAN_POINT('Ctrl Pts',(160.769652108739,-3.94207432655665,339.267916203561));
#69141=CARTESIAN_POINT('Ctrl Pts',(160.491414074466,1.45569917329649,340.624588752396));
#69142=CARTESIAN_POINT('Ctrl Pts',(160.213176040192,5.51759902790003,336.819659221952));
#69143=CARTESIAN_POINT('Ctrl Pts',(159.934938005918,4.51607969422787,331.344855281648));
#69144=CARTESIAN_POINT('Ctrl Pts',(159.656699971644,-0.629779317610128,
329.224323699529));
#69145=CARTESIAN_POINT('Ctrl Pts',(159.37846193737,-5.19769914520483,332.404045009509));
#69146=CARTESIAN_POINT('Ctrl Pts',(159.100223903096,-4.99576718515871,337.966035898031));
#69147=CARTESIAN_POINT('Ctrl Pts',(158.821985868822,-0.209293416695222,
340.806139421548));
#69148=CARTESIAN_POINT('Ctrl Pts',(158.543747834548,4.7692458311037,338.318034496387));
#69149=CARTESIAN_POINT('Ctrl Pts',(158.265509800274,5.37111857365183,332.785018288002));
#69150=CARTESIAN_POINT('Ctrl Pts',(157.987271766,1.04399507873988,329.284658103641));
#69151=CARTESIAN_POINT('Ctrl Pts',(157.709033731726,-4.24118729058956,331.02918281926));
#69152=CARTESIAN_POINT('Ctrl Pts',(157.430795697452,-5.63429468316675,336.417667852479));
#69153=CARTESIAN_POINT('Ctrl Pts',(157.152557663178,-1.85689300705504,340.505180022221));
#69154=CARTESIAN_POINT('Ctrl Pts',(156.874319628904,3.62455197393519,339.540669741894));
#69155=CARTESIAN_POINT('Ctrl Pts',(156.596081594631,5.77979910674458,334.409253859607));
#69156=CARTESIAN_POINT('Ctrl Pts',(156.317843560356,2.63100990898947,329.819956990959));
#69157=CARTESIAN_POINT('Ctrl Pts',(156.039605526083,-2.9322182486027,329.984309134399));
#69158=CARTESIAN_POINT('Ctrl Pts',(155.761367491809,-5.80459299892257,334.751486753724));
#69159=CARTESIAN_POINT('Ctrl Pts',(155.483129457535,-3.35017842978342,339.746721311109));
#69160=CARTESIAN_POINT('Ctrl Pts',(155.204891423261,2.1786454358154,340.385959782779));
#69161=CARTESIAN_POINT('Ctrl Pts',(154.926653388987,5.70815854172035,336.08258245843));
#69162=CARTESIAN_POINT('Ctrl Pts',(154.648415354713,3.9993788061705,330.78573519087));
#69163=CARTESIAN_POINT('Ctrl Pts',(154.370177320439,-1.37957182906757,329.356256536203));
#69164=CARTESIAN_POINT('Ctrl Pts',(154.091939286165,-5.49250975921714,333.105957956745));
#69165=CARTESIAN_POINT('Ctrl Pts',(153.813701251891,-4.56505255264437,338.593793804367));
#69166=CARTESIAN_POINT('Ctrl Pts',(153.535463217617,0.551686001424929,340.783658122032));
#69167=CARTESIAN_POINT('Ctrl Pts',(153.257225183343,5.1621504548586,337.665944747762));
#69168=CARTESIAN_POINT('Ctrl Pts',(152.978987149069,5.03538562908436,332.101733227751));
#69169=CARTESIAN_POINT('Ctrl Pts',(152.700749114795,0.287721733669453,329.197218346285));
#69170=CARTESIAN_POINT('Ctrl Pts',(152.422511080521,-4.72398014996808,331.617830539517));
#69171=CARTESIAN_POINT('Ctrl Pts',(152.144273046247,-5.40055517581262,337.142209725895));
#69172=CARTESIAN_POINT('Ctrl Pts',(151.866035011973,-1.12112042887766,340.700714665783));
#69173=CARTESIAN_POINT('Ctrl Pts',(151.5877969777,4.18714998792789,339.027757899293));
#69174=CARTESIAN_POINT('Ctrl Pts',(151.309558943426,5.65293466304457,333.65858715823));
#69175=CARTESIAN_POINT('Ctrl Pts',(151.031320909152,1.93110463506422,329.52041118284));
#69176=CARTESIAN_POINT('Ctrl Pts',(150.753082874878,-3.56287161345692,330.410772986358));
#69177=CARTESIAN_POINT('Ctrl Pts',(150.474844840604,-5.78725317020745,335.512600683417));
#69178=CARTESIAN_POINT('Ctrl Pts',(150.19660680633,-2.70075791237538,340.144022299277));
#69179=CARTESIAN_POINT('Ctrl Pts',(149.918368772056,2.86418301852214,340.054850576735));
#69180=CARTESIAN_POINT('Ctrl Pts',(149.640130737782,5.80070546859394,335.326917089396));
#69181=CARTESIAN_POINT('Ctrl Pts',(149.361892703508,3.41400612840946,330.298976614406));
#69182=CARTESIAN_POINT('Ctrl Pts',(149.083654669234,-2.10567624516853,329.585095913385));
#69183=CARTESIAN_POINT('Ctrl Pts',(148.80541663496,-5.69301060828579,333.840392768796));
#69184=CARTESIAN_POINT('Ctrl Pts',(148.527178600686,-4.05595316487803,339.159844064509));
#69185=CARTESIAN_POINT('Ctrl Pts',(148.248940566412,1.30319263216773,340.661867861419));
#69186=CARTESIAN_POINT('Ctrl Pts',(147.970702532138,5.46641778576486,336.968079090938));
#69187=CARTESIAN_POINT('Ctrl Pts',(147.692464497864,4.61319202155985,331.468213187502));
#69188=CARTESIAN_POINT('Ctrl Pts',(147.414226463591,-0.473491970228016,
329.209415912808));
#69189=CARTESIAN_POINT('Ctrl Pts',(147.135988429316,-5.12565936966766,332.264552186048));
#69190=CARTESIAN_POINT('Ctrl Pts',(146.857750395043,-5.07408482017158,337.829968543009));
#69191=CARTESIAN_POINT('Ctrl Pts',(146.579512360768,-0.366097524573219,
340.798364538318));
#69192=CARTESIAN_POINT('Ctrl Pts',(146.301274326495,4.67785206573538,338.445686980533));
#69193=CARTESIAN_POINT('Ctrl Pts',(146.023036292221,5.42900586030193,332.930953338969));
#69194=CARTESIAN_POINT('Ctrl Pts',(145.744798257947,1.19804110886455,329.314953279156));
#69195=CARTESIAN_POINT('Ctrl Pts',(145.466560223673,-4.13234828512005,330.916036683908));
#69196=CARTESIAN_POINT('Ctrl Pts',(145.188322189399,-5.67054265121069,336.26491294464));
#69197=CARTESIAN_POINT('Ctrl Pts',(144.910084155125,-2.00496372335765,340.452997266158));
#69198=CARTESIAN_POINT('Ctrl Pts',(144.631846120851,3.50054082020459,339.636946482633));
#69199=CARTESIAN_POINT('Ctrl Pts',(144.353608086577,5.79365072096298,334.565638353212));
#69200=CARTESIAN_POINT('Ctrl Pts',(144.075370052303,2.77001286923813,329.892937495882));
#69201=CARTESIAN_POINT('Ctrl Pts',(143.797132018029,-2.79562490726363,329.906912518462));
#69202=CARTESIAN_POINT('Ctrl Pts',(143.518893983755,-5.79575896972554,334.594738749002));
#69203=CARTESIAN_POINT('Ctrl Pts',(143.240655949481,-3.4772105709325,339.654467247936));
#69204=CARTESIAN_POINT('Ctrl Pts',(142.962417915208,2.03232264526139,340.442859853265));
#69205=CARTESIAN_POINT('Ctrl Pts',(142.684179880933,5.67682336693198,336.236420307731));
#69206=CARTESIAN_POINT('Ctrl Pts',(142.40594184666,4.11178707454463,330.895336095327));
#69207=CARTESIAN_POINT('Ctrl Pts',(142.127703812386,-1.22657552627459,329.321041363502));
#69208=CARTESIAN_POINT('Ctrl Pts',(141.849465778112,-5.43932787085671,332.958243151098));
#69209=CARTESIAN_POINT('Ctrl Pts',(141.571227743838,-4.6604893127014,338.46913506265));
#69210=CARTESIAN_POINT('Ctrl Pts',(141.292989709564,0.395211499010483,340.796452931557));
#69211=CARTESIAN_POINT('Ctrl Pts',(141.01475167529,5.08823255139261,337.80445150068));
#69212=CARTESIAN_POINT('Ctrl Pts',(140.736513641016,5.11185769355109,332.238846321264));
#69213=CARTESIAN_POINT('Ctrl Pts',(140.458275606742,0.444406481233616,329.207111118263));
#69214=CARTESIAN_POINT('Ctrl Pts',(140.180037572468,-4.63086999948305,331.491424539133));
#69215=CARTESIAN_POINT('Ctrl Pts',(139.901799538194,-5.45646543320326,336.995505873951));
#69216=CARTESIAN_POINT('Ctrl Pts',(139.62356150392,-1.27474307617062,340.668340921863));
#69217=CARTESIAN_POINT('Ctrl Pts',(139.345323469646,4.07679218668677,339.139423170357));
#69218=CARTESIAN_POINT('Ctrl Pts',(139.067085435372,5.68711543317582,333.811817873199));
#69219=CARTESIAN_POINT('Ctrl Pts',(138.788847401098,2.0784567883257,329.574589776268));
#69220=CARTESIAN_POINT('Ctrl Pts',(138.510609366824,-3.43757097319903,330.316180562732));
#69221=CARTESIAN_POINT('Ctrl Pts',(138.232371332551,-5.79899059108342,335.356043313715));
#69222=CARTESIAN_POINT('Ctrl Pts',(137.954133298277,-2.83876213649137,340.069170370893));
#69223=CARTESIAN_POINT('Ctrl Pts',(137.675895264003,2.72655643069835,340.130394599535));
#69224=CARTESIAN_POINT('Ctrl Pts',(137.397657229729,5.78975440534314,335.483531428683));
#69225=CARTESIAN_POINT('Ctrl Pts',(137.119419195455,3.53978021883948,330.392938602642));
#69226=CARTESIAN_POINT('Ctrl Pts',(136.841181161181,-1.95859802742279,329.530178020841));
#69227=CARTESIAN_POINT('Ctrl Pts',(136.562943126907,-5.65959977277867,333.686992334875));
#69228=CARTESIAN_POINT('Ctrl Pts',(136.284705092633,-4.16687034221126,339.048734403232));
#69229=CARTESIAN_POINT('Ctrl Pts',(136.006467058359,1.14973449849797,340.695012668966));
#69230=CARTESIAN_POINT('Ctrl Pts',(135.728229024085,5.41124495998901,337.115061866638));
#69231=CARTESIAN_POINT('Ctrl Pts',(135.449990989811,4.70693579154281,331.594150007559));
#69232=CARTESIAN_POINT('Ctrl Pts',(135.171752955537,-0.316858878543813,
329.198736416279));
#69233=CARTESIAN_POINT('Ctrl Pts',(134.893514921263,-5.04987683262017,332.12705678927));
#69234=CARTESIAN_POINT('Ctrl Pts',(134.615276886989,-5.14869735346086,337.691834742175));
#69235=CARTESIAN_POINT('Ctrl Pts',(134.337038852715,-0.522634307678893,
340.786355683602));
#69236=CARTESIAN_POINT('Ctrl Pts',(134.058800818442,4.58304252819027,338.570823420658));
#69237=CARTESIAN_POINT('Ctrl Pts',(133.780562784167,5.48292888153603,333.078399209843));
#69238=CARTESIAN_POINT('Ctrl Pts',(133.502324749894,1.35121232819393,329.349399681374));
#69239=CARTESIAN_POINT('Ctrl Pts',(133.22408671562,-4.02049183487047,330.805872662585));
#69240=CARTESIAN_POINT('Ctrl Pts',(132.945848681346,-5.70264998343651,336.111234396122));
#69241=CARTESIAN_POINT('Ctrl Pts',(132.667610647072,-2.15157041317865,340.396832726132));
#69242=CARTESIAN_POINT('Ctrl Pts',(132.389372612798,3.37397356812602,339.72983732049));
#69243=CARTESIAN_POINT('Ctrl Pts',(132.111134578524,5.80327180572966,334.722340018119));
#69244=CARTESIAN_POINT('Ctrl Pts',(131.83289654425,2.90699316336665,329.969647182866));
#69245=CARTESIAN_POINT('Ctrl Pts',(131.554658509976,-2.65699019786919,329.83323488001));
#69246=CARTESIAN_POINT('Ctrl Pts',(131.276420475702,-5.7826928716315,334.438286666443));
#69247=CARTESIAN_POINT('Ctrl Pts',(130.998182441428,-3.60170364950447,339.558814488204));
#69248=CARTESIAN_POINT('Ctrl Pts',(130.719944407154,1.8845158507141,340.495785542134));
#69249=CARTESIAN_POINT('Ctrl Pts',(130.44170637288,5.64134297014069,336.389355321708));
#69250=CARTESIAN_POINT('Ctrl Pts',(130.163468338606,4.22119291195493,331.007934229403));
#69251=CARTESIAN_POINT('Ctrl Pts',(129.885230304332,-1.07268357682663,329.289972971979));
#69252=CARTESIAN_POINT('Ctrl Pts',(129.606992270059,-5.38217417993802,332.812019238311));
#69253=CARTESIAN_POINT('Ctrl Pts',(129.328754235784,-4.75252297888098,338.341943155101));
#69254=CARTESIAN_POINT('Ctrl Pts',(129.050516201511,0.23844841277096,340.805015165454));
#69255=CARTESIAN_POINT('Ctrl Pts',(128.772278167236,5.0105992155158,337.940910440355));
#69256=CARTESIAN_POINT('Ctrl Pts',(128.494040132963,5.18459707450497,332.377975611908));
#69257=CARTESIAN_POINT('Ctrl Pts',(128.215802098689,0.600766722748434,329.221233863396));
#69258=CARTESIAN_POINT('Ctrl Pts',(127.937564064415,-4.53437838317207,331.367580503998));
#69259=CARTESIAN_POINT('Ctrl Pts',(127.659326030141,-5.50839137417084,336.847344901656));
#69260=CARTESIAN_POINT('Ctrl Pts',(127.381087995867,-1.42743490481644,340.631828149831));
#69261=CARTESIAN_POINT('Ctrl Pts',(127.102849961593,3.96345750778334,339.248065830553));
#69262=CARTESIAN_POINT('Ctrl Pts',(126.824611927319,5.71714346602729,333.965916199926));
#69263=CARTESIAN_POINT('Ctrl Pts',(126.546373893045,2.22429125039721,329.632730009574));
#69264=CARTESIAN_POINT('Ctrl Pts',(126.268135858771,-3.30976021523733,330.225008268662));
#69265=CARTESIAN_POINT('Ctrl Pts',(125.989897824497,-5.80649358332928,335.199225960836));
#69266=CARTESIAN_POINT('Ctrl Pts',(125.711659790223,-2.97469349370475,339.990616929322));
#69267=CARTESIAN_POINT('Ctrl Pts',(125.433421755949,2.58693890868864,340.202192403153));
#69268=CARTESIAN_POINT('Ctrl Pts',(125.155183721675,5.77457565773415,335.639792692846));
#69269=CARTESIAN_POINT('Ctrl Pts',(124.876945687402,3.66296955827404,330.490264671638));
#69270=CARTESIAN_POINT('Ctrl Pts',(124.598707653127,-1.81008963947211,329.479254197684));
#69271=CARTESIAN_POINT('Ctrl Pts',(124.320469618854,-5.62205629195399,333.53455066044));
#69272=CARTESIAN_POINT('Ctrl Pts',(124.04223158458,-4.27474486672454,338.934668352114));
#69273=CARTESIAN_POINT('Ctrl Pts',(123.763993550306,0.995436827567214,340.723998972662));
#69274=CARTESIAN_POINT('Ctrl Pts',(123.485755516032,5.35212083782403,337.260500222085));
#69275=CARTESIAN_POINT('Ctrl Pts',(123.207517481758,4.79724255238381,331.722573782628));
#69276=CARTESIAN_POINT('Ctrl Pts',(122.929279447484,-0.159994416194986,
329.192293008123));
#69277=CARTESIAN_POINT('Ctrl Pts',(122.65104141321,-4.9704068705453,331.991659218448));
#69278=CARTESIAN_POINT('Ctrl Pts',(122.372803378936,-5.21955030288149,337.551735360966));
#69279=CARTESIAN_POINT('Ctrl Pts',(122.094565344662,-0.678789462699493,
340.770121626278));
#69280=CARTESIAN_POINT('Ctrl Pts',(121.816327310388,4.48488644848576,338.693352442011));
#69281=CARTESIAN_POINT('Ctrl Pts',(121.538089276114,5.53284826271111,333.227248235502));
#69282=CARTESIAN_POINT('Ctrl Pts',(121.25985124184,1.50339689095296,329.387972157501));
#69283=CARTESIAN_POINT('Ctrl Pts',(120.981613207566,-3.90569961753098,330.698771197166));
#69284=CARTESIAN_POINT('Ctrl Pts',(120.703375173292,-5.7305932350386,335.956744423159));
#69285=CARTESIAN_POINT('Ctrl Pts',(120.425137139018,-2.2966060241688,340.336727413544));
#69286=CARTESIAN_POINT('Ctrl Pts',(120.146899104744,3.24494263723136,339.819274426487));
#69287=CARTESIAN_POINT('Ctrl Pts',(119.868661070471,5.80865533571912,334.879244430617));
#69288=CARTESIAN_POINT('Ctrl Pts',(119.590423036197,3.04185076822965,330.050030038421));
#69289=CARTESIAN_POINT('Ctrl Pts',(119.312185001923,-2.51641535162041,329.763330018529));
#69290=CARTESIAN_POINT('Ctrl Pts',(119.033946967649,-5.76540424551814,334.28224474751));
#69291=CARTESIAN_POINT('Ctrl Pts',(118.755708933375,-3.72356676053103,339.459832877652));
#69292=CARTESIAN_POINT('Ctrl Pts',(118.477470899101,1.7353329808401,340.544698202998));
#69293=CARTESIAN_POINT('Ctrl Pts',(118.199232864827,5.60174325916709,336.541275827064));
#69294=CARTESIAN_POINT('Ctrl Pts',(117.920994830553,4.32751643015142,331.123447373827));
#69295=CARTESIAN_POINT('Ctrl Pts',(117.642756796279,-0.918008352776408,
329.263074047807));
#69296=CARTESIAN_POINT('Ctrl Pts',(117.364518762005,-5.32109042014236,332.667392991226));
#69297=CARTESIAN_POINT('Ctrl Pts',(117.086280727731,-4.84108634810961,338.212310957373));
#69298=CARTESIAN_POINT('Ctrl Pts',(116.808042693457,0.0815112112657543,
340.809338571572));
#69299=CARTESIAN_POINT('Ctrl Pts',(116.529804659183,4.92930713516613,338.075221924337));
#69300=CARTESIAN_POINT('Ctrl Pts',(116.251566624909,5.25355065757865,332.519019507338));
#69301=CARTESIAN_POINT('Ctrl Pts',(115.973328590636,0.756688283811837,329.239576269243));
#69302=CARTESIAN_POINT('Ctrl Pts',(115.695090556361,-4.43457575930834,331.246388865151));
#69303=CARTESIAN_POINT('Ctrl Pts',(115.416852522088,-5.55629508234218,336.697834996298));
#69304=CARTESIAN_POINT('Ctrl Pts',(115.138614487814,-1.57908441909158,340.591203011347));
#69305=CARTESIAN_POINT('Ctrl Pts',(114.86037645354,3.84722870831154,339.353606548904));
#69306=CARTESIAN_POINT('Ctrl Pts',(114.582138419266,5.74299683509981,334.120769615659));
#69307=CARTESIAN_POINT('Ctrl Pts',(114.303900384992,2.36850153281131,329.694789428705));
#69308=CARTESIAN_POINT('Ctrl Pts',(114.025662350718,-3.17953266711279,330.137322678249));
#69309=CARTESIAN_POINT('Ctrl Pts',(113.747424316444,-5.80975666825273,335.042263132965));
#69310=CARTESIAN_POINT('Ctrl Pts',(113.46918628217,-3.108452726805,339.908419334362));
#69311=CARTESIAN_POINT('Ctrl Pts',(113.190948247896,2.44543240134464,340.270191560766));
#69312=CARTESIAN_POINT('Ctrl Pts',(112.912710213622,5.75518030930339,335.795586779756));
#69313=CARTESIAN_POINT('Ctrl Pts',(112.634472179348,3.78348419373652,330.590883753805));
#69314=CARTESIAN_POINT('Ctrl Pts',(112.356234145074,-1.66025952228718,329.432361628538));
#69315=CARTESIAN_POINT('Ctrl Pts',(112.0779961108,-5.58040758009832,333.383179058555));
#69316=CARTESIAN_POINT('Ctrl Pts',(111.799758076526,-4.37949796833411,338.817729202297));
#69317=CARTESIAN_POINT('Ctrl Pts',(111.521520042252,0.840412287686272,340.748805606682));
#69318=CARTESIAN_POINT('Ctrl Pts',(111.243282007978,5.28908859176198,337.404287958046));
#69319=CARTESIAN_POINT('Ctrl Pts',(110.965043973705,4.88404636199737,331.853390737543));
#69320=CARTESIAN_POINT('Ctrl Pts',(110.686805939431,-0.00301312576609244,
329.19009039332));
#69321=CARTESIAN_POINT('Ctrl Pts',(110.408567905157,-4.88730751248768,331.858458341022));
#69322=CARTESIAN_POINT('Ctrl Pts',(110.130329870883,-5.28659193153996,337.409772700089));
#69323=CARTESIAN_POINT('Ctrl Pts',(109.852091836609,-0.834448964987024,
340.74967422047));
#69324=CARTESIAN_POINT('Ctrl Pts',(109.573853802335,4.38345550028797,338.81318457378));
#69325=CARTESIAN_POINT('Ctrl Pts',(109.295615768061,5.57872755264583,333.377391726243));
#69326=CARTESIAN_POINT('Ctrl Pts',(109.017377733787,1.65448367182431,329.430642541875));
#69327=CARTESIAN_POINT('Ctrl Pts',(108.739139699513,-3.78805545449141,330.594810493246));
#69328=CARTESIAN_POINT('Ctrl Pts',(108.460901665239,-5.75435200182722,335.801555834477));
#69329=CARTESIAN_POINT('Ctrl Pts',(108.182663630965,-2.43996465118251,340.272725217351));
#69330=CARTESIAN_POINT('Ctrl Pts',(107.904425596691,3.11354224603317,339.905192493561));
#69331=CARTESIAN_POINT('Ctrl Pts',(107.626187562417,5.80979737987243,335.036237018951));
#69332=CARTESIAN_POINT('Ctrl Pts',(107.347949528143,3.17448721067152,330.134027366908));
#69333=CARTESIAN_POINT('Ctrl Pts',(107.069711493869,-2.37400301640822,329.697248978614));
#69334=CARTESIAN_POINT('Ctrl Pts',(106.791473459595,-5.74390571555722,334.126726934171));
#69335=CARTESIAN_POINT('Ctrl Pts',(106.513235425322,-3.84271091944876,339.357594692747));
#69336=CARTESIAN_POINT('Ctrl Pts',(106.234997391047,1.58488296911764,340.589562119784));
#69337=CARTESIAN_POINT('Ctrl Pts',(105.956759356774,5.55805314975906,336.692070891295));
#69338=CARTESIAN_POINT('Ctrl Pts',(105.6785213225,4.43067999159659,331.241791180792));
#69339=CARTESIAN_POINT('Ctrl Pts',(105.400283288226,-0.762662798124573,
329.240364232604));
#69340=CARTESIAN_POINT('Ctrl Pts',(105.122045253952,-5.25612119489127,332.524470016072));
#69341=CARTESIAN_POINT('Ctrl Pts',(104.843807219678,-4.92611475132793,338.080333127028));
#69342=CARTESIAN_POINT('Ctrl Pts',(104.565569185404,-0.0754855098054712,
340.809419992954));
#69343=CARTESIAN_POINT('Ctrl Pts',(104.28733115113,4.84441566990115,338.207287878244));
#69344=CARTESIAN_POINT('Ctrl Pts',(104.009093116856,5.31866809279759,332.661875017163));
#69345=CARTESIAN_POINT('Ctrl Pts',(103.730855082582,0.912057310346108,329.262124942162));
#69346=CARTESIAN_POINT('Ctrl Pts',(103.452617048308,-4.33153500386603,331.127938116843));
#69347=CARTESIAN_POINT('Ctrl Pts',(103.174379014034,-5.6001415783824,336.547085330158));
#69348=CARTESIAN_POINT('Ctrl Pts',(102.89614097976,-1.72958088437146,340.546495170927));
#69349=CARTESIAN_POINT('Ctrl Pts',(102.617902945486,3.72819065865516,339.455968259473));
#69350=CARTESIAN_POINT('Ctrl Pts',(102.339664911213,5.76465666223787,334.276265046283));
#69351=CARTESIAN_POINT('Ctrl Pts',(102.061426876938,2.51098233307774,329.760722717809));
#69352=CARTESIAN_POINT('Ctrl Pts',(101.783188842665,-3.04698342110933,330.053187819595));
#69353=CARTESIAN_POINT('Ctrl Pts',(101.504950808391,-5.80877746314596,334.885269444511));
#69354=CARTESIAN_POINT('Ctrl Pts',(101.226712774117,-3.23994216466833,339.822637606779));
#69355=CARTESIAN_POINT('Ctrl Pts',(100.948474739843,2.30214023685744,340.33434241932));
#69356=CARTESIAN_POINT('Ctrl Pts',(100.670236705569,5.73158252255335,335.950799928416));
#69357=CARTESIAN_POINT('Ctrl Pts',(100.391998671295,3.90123612532141,330.694722376988));
#69358=CARTESIAN_POINT('Ctrl Pts',(100.113760637021,-1.50921708196717,329.389534554406));
#69359=CARTESIAN_POINT('Ctrl Pts',(99.8355226027465,-5.53468404914209,333.23298806091));
#69360=CARTESIAN_POINT('Ctrl Pts',(99.5572845684727,-4.48105315622197,338.698002342863));
#69361=CARTESIAN_POINT('Ctrl Pts',(99.2790465341986,0.684774077926888,340.769414457197));
#69362=CARTESIAN_POINT('Ctrl Pts',(99.0008084999249,5.22219424801106,337.546320080579));
#69363=CARTESIAN_POINT('Ctrl Pts',(98.7225704656507,4.96728383615623,331.986505349636));
#69364=CARTESIAN_POINT('Ctrl Pts',(98.444332431377,0.153970364850074,329.192130180225));
#69365=CARTESIAN_POINT('Ctrl Pts',(98.1660943971029,-4.80063943768013,331.727551420403));
#69366=CARTESIAN_POINT('Ctrl Pts',(97.8878563628291,-5.34977328557324,337.266050420816));
#69367=CARTESIAN_POINT('Ctrl Pts',(97.6096183285551,-0.989499151820034,
340.725028396896));
#69368=CARTESIAN_POINT('Ctrl Pts',(97.331380294281,4.27882374857487,338.930232314425));
#69369=CARTESIAN_POINT('Ctrl Pts',(97.0531422600072,5.62053325023763,333.528720047139));
#69370=CARTESIAN_POINT('Ctrl Pts',(96.7749042257333,1.80436234709209,329.477379676539));
#69371=CARTESIAN_POINT('Ctrl Pts',(96.4966661914593,-3.66764524963526,330.494066463036));
#69372=CARTESIAN_POINT('Ctrl Pts',(96.2184281571854,-5.77390893512749,335.645781948935));
#69373=CARTESIAN_POINT('Ctrl Pts',(95.9401901229113,-2.58154161360941,340.204872872023));
#69374=CARTESIAN_POINT('Ctrl Pts',(95.6619520886377,2.97986834322628,339.987528784253));
#69375=CARTESIAN_POINT('Ctrl Pts',(95.3837140543634,5.80669710426784,335.193203146979));
#69376=CARTESIAN_POINT('Ctrl Pts',(95.1054760200898,3.30480563943159,330.221577833395));
#69377=CARTESIAN_POINT('Ctrl Pts',(94.8272379858156,-2.22985718185977,329.63504001271));
#69378=CARTESIAN_POINT('Ctrl Pts',(94.5489999515418,-5.71821297999646,333.971846785681));
#69379=CARTESIAN_POINT('Ctrl Pts',(94.2707619172678,-3.95904912707566,339.252174587916));
#69380=CARTESIAN_POINT('Ctrl Pts',(93.9925238829939,1.43327567429316,340.630344532814));
#69381=CARTESIAN_POINT('Ctrl Pts',(93.71428584872,5.51030454447741,336.841630403699));
#69382=CARTESIAN_POINT('Ctrl Pts',(93.4360478144461,4.5306082661565,331.362879235528));
#69383=CARTESIAN_POINT('Ctrl Pts',(93.1578097801719,-0.606760346347846,
329.221860109099));
#69384=CARTESIAN_POINT('Ctrl Pts',(92.8795717458984,-5.1873139447767,332.383354675345));
#69385=CARTESIAN_POINT('Ctrl Pts',(92.601333711624,-5.00754610071247,337.946106034405));
#69386=CARTESIAN_POINT('Ctrl Pts',(92.3230956773503,-0.232427111283864,
340.805259370145));
#69387=CARTESIAN_POINT('Ctrl Pts',(92.0448576430763,4.75598680755151,338.33701186739));
#69388=CARTESIAN_POINT('Ctrl Pts',(91.7666196088024,5.37990183134708,332.806437828148));
#69389=CARTESIAN_POINT('Ctrl Pts',(91.4883815745285,1.06676035173629,329.288863417088));
#69390=CARTESIAN_POINT('Ctrl Pts',(91.2101435402544,-4.22533135730589,331.01231475193));
#69391=CARTESIAN_POINT('Ctrl Pts',(90.9319055059806,-5.63989884553708,336.395205980787));
#69392=CARTESIAN_POINT('Ctrl Pts',(90.6536674717066,-1.87881440798938,340.497737274284));
#69393=CARTESIAN_POINT('Ctrl Pts',(90.3754294374327,3.60643028051496,339.555076217639));
#69394=CARTESIAN_POINT('Ctrl Pts',(90.0971914031586,5.78210713141441,334.432288948882));
#69395=CARTESIAN_POINT('Ctrl Pts',(89.8189533688849,2.65162961157622,329.830481732335));
#69396=CARTESIAN_POINT('Ctrl Pts',(89.5407153346108,-2.91220926481656,329.972665128059));
#69397=CARTESIAN_POINT('Ctrl Pts',(89.262477300337,-5.80355668302547,334.728359532423));
#69398=CARTESIAN_POINT('Ctrl Pts',(88.984239266063,-3.36906579357812,339.733334384476));
#69399=CARTESIAN_POINT('Ctrl Pts',(88.7060012317891,2.15716704730625,340.394598135795));
#69400=CARTESIAN_POINT('Ctrl Pts',(88.4277631975151,5.70379952861112,336.105318802034));
#69401=CARTESIAN_POINT('Ctrl Pts',(88.1495251632412,4.01613937045259,330.801704718125));
#69402=CARTESIAN_POINT('Ctrl Pts',(87.8712871289672,-1.35707260985033,329.350804247655));
#69403=CARTESIAN_POINT('Ctrl Pts',(87.5930490946932,-5.48491908645251,333.084087337121));
#69404=CARTESIAN_POINT('Ctrl Pts',(87.3148110604194,-4.57933627469021,338.575575198485));
#69405=CARTESIAN_POINT('Ctrl Pts',(87.0365730261455,0.528635845462655,340.785810475604));
#69406=CARTESIAN_POINT('Ctrl Pts',(86.7583349918715,5.15148665288674,337.686492877684));
#69407=CARTESIAN_POINT('Ctrl Pts',(86.4800969575976,5.04689419477502,332.121820418482));
#69408=CARTESIAN_POINT('Ctrl Pts',(86.2018589233236,0.310841426154469,329.19841087938));
#69409=CARTESIAN_POINT('Ctrl Pts',(85.9236208890498,-4.71046593123611,331.599034044954));
#69410=CARTESIAN_POINT('Ctrl Pts',(85.6453828547757,-5.40904822989449,337.120673469299));
#69411=CARTESIAN_POINT('Ctrl Pts',(85.3671448205018,-1.1438268053997,340.696202151958));
#69412=CARTESIAN_POINT('Ctrl Pts',(85.0889067862279,4.17106759555441,339.04441019557));
#69413=CARTESIAN_POINT('Ctrl Pts',(84.8106687519538,5.65823482892504,333.681122698105));
#69414=CARTESIAN_POINT('Ctrl Pts',(84.53243071768,1.95292347520033,329.528149433992));
#69415=CARTESIAN_POINT('Ctrl Pts',(84.2541926834061,-3.54455692661247,330.396612669922));
#69416=CARTESIAN_POINT('Ctrl Pts',(83.9759546491321,-5.7892497544475,335.48953651278));
#69417=CARTESIAN_POINT('Ctrl Pts',(83.6977166148583,-2.72123353181235,340.133219923406));
#69418=CARTESIAN_POINT('Ctrl Pts',(83.419478580584,2.8440185376259,340.066223176525));
#69419=CARTESIAN_POINT('Ctrl Pts',(83.1412405463105,5.79935677272967,335.350028197878));
#69420=CARTESIAN_POINT('Ctrl Pts',(82.8630025120362,3.43271089586507,330.312617508446));
#69421=CARTESIAN_POINT('Ctrl Pts',(82.5847644777625,-2.08408310340512,329.576748545861));
#69422=CARTESIAN_POINT('Ctrl Pts',(82.3065264434884,-5.68834479969662,333.817717395679));
#69423=CARTESIAN_POINT('Ctrl Pts',(82.0282884092145,-4.07249643313815,339.14364954102));
#69424=CARTESIAN_POINT('Ctrl Pts',(81.7500503749407,1.28062180016229,340.667015662733));
#69425=CARTESIAN_POINT('Ctrl Pts',(81.4718123406666,5.45853230940055,336.989845155771));
#69426=CARTESIAN_POINT('Ctrl Pts',(81.1935743063928,4.627228286107,331.486623119424));
#69427=CARTESIAN_POINT('Ctrl Pts',(80.9153362721188,-0.450414837569424,
329.207575189023));
#69428=CARTESIAN_POINT('Ctrl Pts',(80.6370982378449,-5.11471891292048,332.244150011606));
#69429=CARTESIAN_POINT('Ctrl Pts',(80.358860203571,-5.08532093501182,337.809727692259));
#69430=CARTESIAN_POINT('Ctrl Pts',(80.080622169297,-0.389198994256777,340.796859741237));
#69431=CARTESIAN_POINT('Ctrl Pts',(79.802384135023,4.66408511895998,338.464299167193));
#69432=CARTESIAN_POINT('Ctrl Pts',(79.5241461007491,5.43720716029067,332.952602380386));
#69433=CARTESIAN_POINT('Ctrl Pts',(79.2459080664751,1.22068444366876,329.319772169561));
#69434=CARTESIAN_POINT('Ctrl Pts',(78.9676700322012,-4.11604236963513,330.899603198703));
#69435=CARTESIAN_POINT('Ctrl Pts',(78.6894319979273,-5.67553785301064,336.24230785064));
#69436=CARTESIAN_POINT('Ctrl Pts',(78.4111939636534,-2.02667601947968,340.444964924476));
#69437=CARTESIAN_POINT('Ctrl Pts',(78.1329559293794,3.48203648343876,339.650858054674));
#69438=CARTESIAN_POINT('Ctrl Pts',(77.8547178951055,5.79533550027971,334.588727394648));
#69439=CARTESIAN_POINT('Ctrl Pts',(77.5764798608315,2.79034066752573,329.904015534182));
#69440=CARTESIAN_POINT('Ctrl Pts',(77.2982418265576,-2.77530861045587,329.895813401389));
#69441=CARTESIAN_POINT('Ctrl Pts',(77.0200037922837,-5.79409814011006,334.571647972472));
#69442=CARTESIAN_POINT('Ctrl Pts',(76.7417657580097,-3.49572932733361,339.640574876751));
#69443=CARTESIAN_POINT('Ctrl Pts',(76.4635277237358,2.0106186922566,340.45091471141));
#69444=CARTESIAN_POINT('Ctrl Pts',(76.1852896894618,5.67185161464618,336.259030570777));
#69445=CARTESIAN_POINT('Ctrl Pts',(75.9070516551879,4.12811002666756,330.911752658603));
#69446=CARTESIAN_POINT('Ctrl Pts',(75.628813620914,-1.20393720197976,329.316198989197));
#69447=CARTESIAN_POINT('Ctrl Pts',(75.35057558664,-5.43114903045424,332.93658561464));
#69448=CARTESIAN_POINT('Ctrl Pts',(75.0723375523661,-4.67427555730914,338.450537165582));
#69449=CARTESIAN_POINT('Ctrl Pts',(74.7940995180922,0.372111602584409,340.797981689513));
#69450=CARTESIAN_POINT('Ctrl Pts',(74.5158614838182,5.07701743714451,337.82470399505));
#69451=CARTESIAN_POINT('Ctrl Pts',(74.2376234495443,5.12281930629161,332.25923713689));
#69452=CARTESIAN_POINT('Ctrl Pts',(73.9593854152703,0.467485510743936,329.208927904614));
#69453=CARTESIAN_POINT('Ctrl Pts',(73.6811473809965,-4.61685283793864,331.473000058189));
#69454=CARTESIAN_POINT('Ctrl Pts',(73.4029093467224,-5.46437348188109,336.973747999931));
#69455=CARTESIAN_POINT('Ctrl Pts',(73.1246713124486,-1.29731923552167,340.663216534608));
#69456=CARTESIAN_POINT('Ctrl Pts',(72.8464332781745,4.06026572487547,339.155634844415));
#69457=CARTESIAN_POINT('Ctrl Pts',(72.5681952439007,5.69180475897825,333.834488394571));
#69458=CARTESIAN_POINT('Ctrl Pts',(72.2899572096266,2.10005857666722,329.582914742107));
#69459=CARTESIAN_POINT('Ctrl Pts',(72.0117191753529,-3.41888036463754,330.302520274763));
#69460=CARTESIAN_POINT('Ctrl Pts',(71.7334811410787,-5.80036325790589,335.332933616582));
#69461=CARTESIAN_POINT('Ctrl Pts',(71.455243106805,-2.85893840261536,340.057818692555));
#69462=CARTESIAN_POINT('Ctrl Pts',(71.1770050725308,2.70609202689364,340.141218207653));
#69463=CARTESIAN_POINT('Ctrl Pts',(70.8987670382572,5.78778174517512,335.506597657843));
#69464=CARTESIAN_POINT('Ctrl Pts',(70.620529003983,3.55810958342815,330.407079914801));
#69465=CARTESIAN_POINT('Ctrl Pts',(70.3422909697092,-1.93678722541939,329.522417142556));
#69466=CARTESIAN_POINT('Ctrl Pts',(70.0640529354351,-5.65432298443225,333.664451309597));
#69467=CARTESIAN_POINT('Ctrl Pts',(69.7858149011614,-4.18296999830208,339.032098797155));
#69468=CARTESIAN_POINT('Ctrl Pts',(69.5075768668872,1.12703281473394,340.699548732244));
#69469=CARTESIAN_POINT('Ctrl Pts',(69.2293388326135,5.4027742486657,337.136606920955));
#69470=CARTESIAN_POINT('Ctrl Pts',(68.9511007983393,4.72046949941413,331.61293247457));
#69471=CARTESIAN_POINT('Ctrl Pts',(68.6728627640656,-0.293740435434174,
329.197519903239));
#69472=CARTESIAN_POINT('Ctrl Pts',(68.3946247297915,-5.03838910828626,332.106957672239));
#69473=CARTESIAN_POINT('Ctrl Pts',(68.1163866955177,-5.15938246296538,337.67129768419));
#69474=CARTESIAN_POINT('Ctrl Pts',(67.8381486612436,-0.545686683741498,
340.78422723965));
#69475=CARTESIAN_POINT('Ctrl Pts',(67.5599106269698,4.56877771082971,338.589056832337));
#69476=CARTESIAN_POINT('Ctrl Pts',(67.2816725926958,5.49054223522097,333.10026194438));
#69477=CARTESIAN_POINT('Ctrl Pts',(67.0034345584219,1.37371719062049,329.354828629979));
#69478=CARTESIAN_POINT('Ctrl Pts',(66.7251965241479,-4.00374784377992,330.789885759252));
#69479=CARTESIAN_POINT('Ctrl Pts',(66.446958489874,-5.7070325771648,336.088502586077));
#69480=CARTESIAN_POINT('Ctrl Pts',(66.1687204556001,-2.1730577501483,340.388216655929));
#69481=CARTESIAN_POINT('Ctrl Pts',(65.8904824213261,3.35510009989947,339.743243830584));
#69482=CARTESIAN_POINT('Ctrl Pts',(65.6122443870522,5.8043321094658,334.745466152075));
#69483=CARTESIAN_POINT('Ctrl Pts',(65.3340063527783,2.92701421397687,329.981270428894));
#69484=CARTESIAN_POINT('Ctrl Pts',(65.0557683185043,-2.63638142301966,329.822688756789));
#69485=CARTESIAN_POINT('Ctrl Pts',(64.7775302842304,-5.78040874103706,334.415249195591));
#69486=CARTESIAN_POINT('Ctrl Pts',(64.4992922499564,-3.61984027609792,339.54442681669));
#69487=CARTESIAN_POINT('Ctrl Pts',(64.2210542156825,1.86260218146139,340.503251023743));
#69488=CARTESIAN_POINT('Ctrl Pts',(63.9428161814086,5.63576210905672,336.411822994159));
#69489=CARTESIAN_POINT('Ctrl Pts',(63.6645781471346,4.23706633288306,331.024785841308));
#69490=CARTESIAN_POINT('Ctrl Pts',(63.3863401128608,-1.04992267798081,329.285744047825));
#69491=CARTESIAN_POINT('Ctrl Pts',(63.1081020785866,-5.37341314409502,332.790590599372));
#69492=CARTESIAN_POINT('Ctrl Pts',(62.8298640443129,-4.76580167932123,338.322979547047));
#69493=CARTESIAN_POINT('Ctrl Pts',(62.5516260100388,0.21531564344817,340.805919211494));
#69494=CARTESIAN_POINT('Ctrl Pts',(62.2733879757649,4.99884097827888,337.960852510781));
#69495=CARTESIAN_POINT('Ctrl Pts',(61.995149941491,5.19500373011495,332.398655163035));
#69496=CARTESIAN_POINT('Ctrl Pts',(61.716911907217,0.623788236953903,329.223673576385));
#69497=CARTESIAN_POINT('Ctrl Pts',(61.4386738729432,-4.51986851416046,331.349541490248));
#69498=CARTESIAN_POINT('Ctrl Pts',(61.1604358386692,-5.51570864297967,336.825381297832));
#69499=CARTESIAN_POINT('Ctrl Pts',(60.8821978043952,-1.44986436186256,340.626095630978));
#69500=CARTESIAN_POINT('Ctrl Pts',(60.6039597701214,3.94649904417292,339.263825044612));
#69501=CARTESIAN_POINT('Ctrl Pts',(60.3257217358473,5.72121852760133,333.988705148759));
#69502=CARTESIAN_POINT('Ctrl Pts',(60.0474837015735,2.2456602132971,329.641635611203));
#69503=CARTESIAN_POINT('Ctrl Pts',(59.7692456672994,-3.2907073328593,330.211857983917));
#69504=CARTESIAN_POINT('Ctrl Pts',(59.4910076330256,-5.80724133041153,335.17608761193));
#69505=CARTESIAN_POINT('Ctrl Pts',(59.2127695987516,-2.99455567378668,339.978724237523));
#69506=CARTESIAN_POINT('Ctrl Pts',(58.9345315644777,2.56618952510292,340.212459116192));
#69507=CARTESIAN_POINT('Ctrl Pts',(58.6562935302037,5.77198047370087,335.6627971997));
#69508=CARTESIAN_POINT('Ctrl Pts',(58.3780554959298,3.68091013587568,330.504896075916));
#69509=CARTESIAN_POINT('Ctrl Pts',(58.0998174616558,-1.78807710349808,329.472085475637));
#69510=CARTESIAN_POINT('Ctrl Pts',(57.821579427382,-5.61617237696643,333.512160442483));
#69511=CARTESIAN_POINT('Ctrl Pts',(57.543341393108,-4.2903891546611,338.917603810785));
#69512=CARTESIAN_POINT('Ctrl Pts',(57.265103358834,0.972620868836612,340.727919985669));
#69513=CARTESIAN_POINT('Ctrl Pts',(56.9868653245601,5.34307107686344,337.281808533663));
#69514=CARTESIAN_POINT('Ctrl Pts',(56.7086272902862,4.81026382125253,331.741715069755));
#69515=CARTESIAN_POINT('Ctrl Pts',(56.4303892560122,-0.136851543744224,
329.191701594125));
#69516=CARTESIAN_POINT('Ctrl Pts',(56.1521512217384,-4.95838026697236,331.971877835222));
#69517=CARTESIAN_POINT('Ctrl Pts',(55.8739131874643,-5.22967660477275,337.530917091927));
#69518=CARTESIAN_POINT('Ctrl Pts',(55.5956751531904,-0.701775912273333,
340.767371089645));
#69519=CARTESIAN_POINT('Ctrl Pts',(55.3174371189165,4.47013417672383,338.711193764654));
#69520=CARTESIAN_POINT('Ctrl Pts',(55.0391990846425,5.53986811081383,333.24930869897));
#69521=CARTESIAN_POINT('Ctrl Pts',(54.7609610503686,1.52574684792925,329.39400720008));
#69522=CARTESIAN_POINT('Ctrl Pts',(54.4827230160947,-3.88852977731343,330.683242549359));
#69523=CARTESIAN_POINT('Ctrl Pts',(54.2044849818207,-5.73436002052102,335.933902495856));
#69524=CARTESIAN_POINT('Ctrl Pts',(53.9262469475468,-2.31785271191163,340.327533906283));
#69525=CARTESIAN_POINT('Ctrl Pts',(53.6480089132729,3.22571381896912,339.832166085187));
#69526=CARTESIAN_POINT('Ctrl Pts',(53.3697708789989,5.80909038963983,334.902390770369));
#69527=CARTESIAN_POINT('Ctrl Pts',(53.0915328447249,3.06155045177167,330.062190004873));
#69528=CARTESIAN_POINT('Ctrl Pts',(52.8132948104511,-2.49552914727676,329.753344589951));
#69529=CARTESIAN_POINT('Ctrl Pts',(52.535056776177,-5.76249848181913,334.259277404323));
#69530=CARTESIAN_POINT('Ctrl Pts',(52.2568187419033,-3.74130801393427,339.444960411701));
#69531=CARTESIAN_POINT('Ctrl Pts',(51.9785807076291,1.71322559672231,340.551568856769));
#69532=CARTESIAN_POINT('Ctrl Pts',(51.7003426733553,5.59555736443519,336.563584503002));
#69533=CARTESIAN_POINT('Ctrl Pts',(51.4221046390813,4.3429287290972,331.1407217293));
#69534=CARTESIAN_POINT('Ctrl Pts',(51.1438666048075,-0.895141499410306,
329.259461661765));
#69535=CARTESIAN_POINT('Ctrl Pts',(50.8656285705334,-5.31175358617586,332.646208897021));
#69536=CARTESIAN_POINT('Ctrl Pts',(50.5873905362596,-4.85384780826223,338.192995485581));
#69537=CARTESIAN_POINT('Ctrl Pts',(50.3091525019856,0.0583624606174229,
340.809617245559));
#69538=CARTESIAN_POINT('Ctrl Pts',(50.0309144677117,4.91701436081699,338.094839009098));
#69539=CARTESIAN_POINT('Ctrl Pts',(49.7526764334377,5.26339475710779,332.539972693736));
#69540=CARTESIAN_POINT('Ctrl Pts',(49.4744383991637,0.779635472380057,329.242637127389));
#69541=CARTESIAN_POINT('Ctrl Pts',(49.1962003648898,-4.41958377795016,331.2287484907));
#69542=CARTESIAN_POINT('Ctrl Pts',(48.9179623306159,-5.56301622820511,336.675681700515));
#69543=CARTESIAN_POINT('Ctrl Pts',(48.639724296342,-1.60135079582141,340.584866546789));
#69544=CARTESIAN_POINT('Ctrl Pts',(48.361486262068,3.8298506259886,339.368901795568));
#69545=CARTESIAN_POINT('Ctrl Pts',(48.0832482277942,5.74645465683156,334.143660351442));
#69546=CARTESIAN_POINT('Ctrl Pts',(47.80501019352,2.3896220666319,329.704269163243));
#69547=CARTESIAN_POINT('Ctrl Pts',(47.5267721592463,-3.16013142335197,330.124691999078));
#69548=CARTESIAN_POINT('Ctrl Pts',(47.2485341249722,-5.80987894958908,335.01911302793));
#69549=CARTESIAN_POINT('Ctrl Pts',(46.9702960906984,-3.12798631746102,339.89599431316));
#69550=CARTESIAN_POINT('Ctrl Pts',(46.6920580564244,2.42441318919865,340.27989388196));
#69551=CARTESIAN_POINT('Ctrl Pts',(46.4138200221505,5.75196449641075,335.81851276639));
#69552=CARTESIAN_POINT('Ctrl Pts',(46.1355819878765,3.80102288412349,330.605994566335));
#69553=CARTESIAN_POINT('Ctrl Pts',(45.8573439536026,-1.63806132591808,329.425790297338));
#69554=CARTESIAN_POINT('Ctrl Pts',(45.5791059193286,-5.57392083491017,333.360955997275));
#69555=CARTESIAN_POINT('Ctrl Pts',(45.3008678850548,-4.39467546464187,338.800248186262));
#69556=CARTESIAN_POINT('Ctrl Pts',(45.0226298507807,0.817498714224755,340.752108706288));
#69557=CARTESIAN_POINT('Ctrl Pts',(44.7443918165069,5.27946638930855,337.425343967539));
#69558=CARTESIAN_POINT('Ctrl Pts',(44.4661537822328,4.89654568372007,331.872876867797));
#69559=CARTESIAN_POINT('Ctrl Pts',(44.187915747959,0.0201372770774963,329.190124510216));
#69560=CARTESIAN_POINT('Ctrl Pts',(43.909677713685,-4.87475081151337,331.839009135989));
#69561=CARTESIAN_POINT('Ctrl Pts',(43.6314396794111,-5.29615203158245,337.388688421515));
#69562=CARTESIAN_POINT('Ctrl Pts',(43.3532016451371,-0.857352703344343,
340.7463035996));
#69563=CARTESIAN_POINT('Ctrl Pts',(43.0749636108633,4.36822654624751,338.830620779635));
#69564=CARTESIAN_POINT('Ctrl Pts',(42.7967255765892,5.58514876926659,333.399633810069));
#69565=CARTESIAN_POINT('Ctrl Pts',(42.5184875423154,1.67666240339047,329.437279271636));
#69566=CARTESIAN_POINT('Ctrl Pts',(42.2402495080414,-3.77047230258058,330.579751439999));
#69567=CARTESIAN_POINT('Ctrl Pts',(41.9620114737676,-5.7575002285534,335.778620469114));
#69568=CARTESIAN_POINT('Ctrl Pts',(41.6837734394935,-2.46095517534683,340.262960986141));
#69569=CARTESIAN_POINT('Ctrl Pts',(41.4055354052196,3.09397211863666,339.917559887364));
#69570=CARTESIAN_POINT('Ctrl Pts',(41.1272973709457,5.80960686630092,335.059386663018));
#69571=CARTESIAN_POINT('Ctrl Pts',(40.8490593366717,3.19385114241758,330.146715174566));
#69572=CARTESIAN_POINT('Ctrl Pts',(40.5708213023978,-2.35285463369676,329.687831536048));
#69573=CARTESIAN_POINT('Ctrl Pts',(40.2925832681238,-5.74038044054507,334.103846489421));
#69574=CARTESIAN_POINT('Ctrl Pts',(40.0143452338499,-3.86004384498157,339.342248292249));
#69575=CARTESIAN_POINT('Ctrl Pts',(39.736107199576,1.56259801296774,340.595832928758));
#69576=CARTESIAN_POINT('Ctrl Pts',(39.457869165302,5.55126673832543,336.714204280906));
#69577=CARTESIAN_POINT('Ctrl Pts',(39.1796311310281,4.44561991448462,331.259475666079));
#69578=CARTESIAN_POINT('Ctrl Pts',(38.9013930967542,-0.739706687636357,
329.237371022444));
#69579=CARTESIAN_POINT('Ctrl Pts',(38.6231550624802,-5.24621538056624,332.503545935245));
#69580=CARTESIAN_POINT('Ctrl Pts',(38.3449170282063,-4.9383496527626,338.060679895673));
#69581=CARTESIAN_POINT('Ctrl Pts',(38.0666789939323,-0.0986333385400925,
340.809073091401));
#69582=CARTESIAN_POINT('Ctrl Pts',(37.7884409596584,4.83159733463496,338.226565652931));
#69583=CARTESIAN_POINT('Ctrl Pts',(37.5102029253845,5.32794244807527,332.683086538794));
#69584=CARTESIAN_POINT('Ctrl Pts',(37.2319648911105,0.93491341721853,329.265804710423));
#69585=CARTESIAN_POINT('Ctrl Pts',(36.9537268568366,-4.31607185732023,331.11070926271));
#69586=CARTESIAN_POINT('Ctrl Pts',(36.6754888225627,-5.60626169351242,336.524758518774));
#69587=CARTESIAN_POINT('Ctrl Pts',(36.3972507882887,-1.7516679218552,340.539559387556));
#69588=CARTESIAN_POINT('Ctrl Pts',(36.1190127540148,3.71040564711238,339.470788370142));
#69589=CARTESIAN_POINT('Ctrl Pts',(35.8407747197408,5.76749471922252,334.299240854176));
#69590=CARTESIAN_POINT('Ctrl Pts',(35.5625366854669,2.53183901558466,329.770769663146));
#69591=CARTESIAN_POINT('Ctrl Pts',(35.2842986511929,-3.02724798277262,330.041085968933));
#69592=CARTESIAN_POINT('Ctrl Pts',(35.0060606169191,-5.80827418944645,334.862124487579));
#69593=CARTESIAN_POINT('Ctrl Pts',(34.7278225826451,-3.25913290245178,339.809689328935));
#69594=CARTESIAN_POINT('Ctrl Pts',(34.4495845483711,2.28086654440011,340.343473264026));
#69595=CARTESIAN_POINT('Ctrl Pts',(34.1713465140972,5.72774842899101,335.973630654255));
#69596=CARTESIAN_POINT('Ctrl Pts',(33.8931084798233,3.91836012172512,330.710301563841));
#69597=CARTESIAN_POINT('Ctrl Pts',(33.6148704455493,-1.48684943434735,329.383565412443));
#69598=CARTESIAN_POINT('Ctrl Pts',(33.3366324112754,-5.52759921038091,333.21094838361));
#69599=CARTESIAN_POINT('Ctrl Pts',(33.0583943770014,-4.49575277827853,338.680117616777));
#69600=CARTESIAN_POINT('Ctrl Pts',(32.7801563427275,0.661779621247826,340.772097231476));
#69601=CARTESIAN_POINT('Ctrl Pts',(32.5019183084535,5.21200663020625,337.567108412865));
#69602=CARTESIAN_POINT('Ctrl Pts',(32.2236802741797,4.97925208371616,332.006322094225));
#69603=CARTESIAN_POINT('Ctrl Pts',(31.9454422399056,0.177111393640036,329.192789803102));
#69604=CARTESIAN_POINT('Ctrl Pts',(31.6672042056318,-4.78756180821967,331.70844859539));
#69605=CARTESIAN_POINT('Ctrl Pts',(31.3889661713578,-5.35876020297263,337.244715528469));
#69606=CARTESIAN_POINT('Ctrl Pts',(31.1107281370839,-1.01230345462855,340.72104015302));
#69607=CARTESIAN_POINT('Ctrl Pts',(30.8324901028099,4.26312923245365,338.947250671558));
#69608=CARTESIAN_POINT('Ctrl Pts',(30.554252068536,5.62635114659746,333.551127510132));
#69609=CARTESIAN_POINT('Ctrl Pts',(30.276014034262,1.82635365831559,329.484613247335));
#69610=CARTESIAN_POINT('Ctrl Pts',(29.9977759999882,-3.6496616252667,330.479488000484));
#69611=CARTESIAN_POINT('Ctrl Pts',(29.7195379657141,-5.77643630425902,335.622769892941));
#69612=CARTESIAN_POINT('Ctrl Pts',(29.4412999314403,-2.60226064689294,340.194545046715));
#69613=CARTESIAN_POINT('Ctrl Pts',(29.1630618971662,2.95997119682261,339.999362882477));
#69614=CARTESIAN_POINT('Ctrl Pts',(28.8848238628924,5.80588116231729,335.216339191467));
#69615=CARTESIAN_POINT('Ctrl Pts',(28.6065858286184,3.32381967981889,330.234784217607));
#69616=CARTESIAN_POINT('Ctrl Pts',(28.3283477943445,-2.20846206335126,329.626197432781));
#69617=CARTESIAN_POINT('Ctrl Pts',(28.0501097600705,-5.71407076783057,333.949069946695));
#69618=CARTESIAN_POINT('Ctrl Pts',(27.7718717257966,-3.97596106821805,339.236365458825));
#69619=CARTESIAN_POINT('Ctrl Pts',(27.4936336915227,1.410829418609,340.636010918044));
#69620=CARTESIAN_POINT('Ctrl Pts',(27.2153956572488,5.50292257178667,336.863572345158));
#69621=CARTESIAN_POINT('Ctrl Pts',(26.9371576229748,4.54506490383972,331.380960937403));
#69622=CARTESIAN_POINT('Ctrl Pts',(26.6589195887009,-0.583731741312921,
329.219488260466));
#69623=CARTESIAN_POINT('Ctrl Pts',(26.3806815544269,-5.17684638332907,332.362705886685));
#69624=CARTESIAN_POINT('Ctrl Pts',(26.102443520153,-5.01924550949151,337.926129394297));
#69625=CARTESIAN_POINT('Ctrl Pts',(25.824205485879,-0.255557115535859,340.804287146361));
#69626=CARTESIAN_POINT('Ctrl Pts',(25.5459674516051,4.74265227133019,338.355936255349));
#69627=CARTESIAN_POINT('Ctrl Pts',(25.2677294173311,5.38859967022931,332.82789219634));
#69628=CARTESIAN_POINT('Ctrl Pts',(24.9894913830572,1.08950868735974,329.293159408492));
#69629=CARTESIAN_POINT('Ctrl Pts',(24.7112533487833,-4.20940833677799,330.995509998641));
#69630=CARTESIAN_POINT('Ctrl Pts',(24.4330153145093,-5.64541346101978,336.372721956863));
#69631=CARTESIAN_POINT('Ctrl Pts',(24.1547772802354,-1.90070597824981,340.490207236613));
#69632=CARTESIAN_POINT('Ctrl Pts',(23.8765392459615,3.58825132638577,339.56941037065));
#69633=CARTESIAN_POINT('Ctrl Pts',(23.5983012116875,5.78432335129987,334.455333051928));
#69634=CARTESIAN_POINT('Ctrl Pts',(23.3200631774136,2.67220721319882,329.841088552181));
#69635=CARTESIAN_POINT('Ctrl Pts',(23.0418251431397,-2.89215404274099,329.961100942688));
#69636=CARTESIAN_POINT('Ctrl Pts',(22.7635871088657,-5.80242822178108,334.705236624064));
#69637=CARTESIAN_POINT('Ctrl Pts',(22.4853490745917,-3.38789966539284,339.719872304835));
#69638=CARTESIAN_POINT('Ctrl Pts',(22.2071110403179,2.13565440860932,340.40315083666));
#69639=CARTESIAN_POINT('Ctrl Pts',(21.9288730060438,5.6993499540381,336.128037596058));
#69640=CARTESIAN_POINT('Ctrl Pts',(21.65063497177,4.03283616891361,330.817740903362));
#69641=CARTESIAN_POINT('Ctrl Pts',(21.372396937496,-1.3345518438582,329.345441653607));
#69642=CARTESIAN_POINT('Ctrl Pts',(21.0941589032221,-5.47724132747451,333.062247137192));
#69643=CARTESIAN_POINT('Ctrl Pts',(20.8159208689482,-4.5935472888171,338.557299821791));
#69644=CARTESIAN_POINT('Ctrl Pts',(20.5376828346742,0.505577296140925,340.787870965592));
#69645=CARTESIAN_POINT('Ctrl Pts',(20.2594448004003,5.14074105873908,337.706998353104));
#69646=CARTESIAN_POINT('Ctrl Pts',(19.9812067661263,5.05832262894602,332.141953307203));
#69647=CARTESIAN_POINT('Ctrl Pts',(19.7029687318525,0.33395618328883,329.199695526581));
#69648=CARTESIAN_POINT('Ctrl Pts',(19.4247306975784,-4.69687692258734,331.580291548863));
#69649=CARTESIAN_POINT('Ctrl Pts',(19.1464926633046,-5.41745540239484,337.099103541939));
#69650=CARTESIAN_POINT('Ctrl Pts',(18.8682546290305,-1.16651502093527,340.691599197295));
#69651=CARTESIAN_POINT('Ctrl Pts',(18.5900165947567,4.15491897750313,339.06099827716));
#69652=CARTESIAN_POINT('Ctrl Pts',(18.3117785604827,5.66344515679048,333.703679178312));
#69653=CARTESIAN_POINT('Ctrl Pts',(18.0335405262088,1.97471130800469,329.535974563863));
#69654=CARTESIAN_POINT('Ctrl Pts',(17.7553024919348,-3.52618596144585,330.382525443273));
#69655=CARTESIAN_POINT('Ctrl Pts',(17.4770644576609,-5.79115442049705,335.46646456958));
#69656=CARTESIAN_POINT('Ctrl Pts',(17.198826423387,-2.74166594515719,340.122336045387));
#69657=CARTESIAN_POINT('Ctrl Pts',(16.920588389113,2.82380890113031,340.0775153379));
#69658=CARTESIAN_POINT('Ctrl Pts',(16.6423503548391,5.79791599820176,335.373133748825));
#69659=CARTESIAN_POINT('Ctrl Pts',(16.3641123205652,3.45136116082296,330.326332825898));
#69660=CARTESIAN_POINT('Ctrl Pts',(16.0858742862912,-2.06245687183517,329.56848728543));
#69661=CARTESIAN_POINT('Ctrl Pts',(15.8076362520173,-5.68358867502499,333.795060794126));
#69662=CARTESIAN_POINT('Ctrl Pts',(15.5293982177433,-4.08897504077325,339.12738922718));
#69663=CARTESIAN_POINT('Ctrl Pts',(15.2511601834694,1.25803063521879,340.672073486614));
#69664=CARTESIAN_POINT('Ctrl Pts',(14.9729221491955,5.45056016578104,337.011579627053));
#69665=CARTESIAN_POINT('Ctrl Pts',(14.6946841149215,4.64119108232566,331.505088834606));
#69666=CARTESIAN_POINT('Ctrl Pts',(14.4164460806476,-0.427330553480647,
329.205826433848));
#69667=CARTESIAN_POINT('Ctrl Pts',(14.1382080463736,-5.10369724780541,332.223791592866));
#69668=CARTESIAN_POINT('Ctrl Pts',(13.8599700120997,-5.09647630815562,337.789442230377));
#69669=CARTESIAN_POINT('Ctrl Pts',(13.5817319778257,-0.412294284588803,
340.795262905107));
#69670=CARTESIAN_POINT('Ctrl Pts',(13.3034939435518,4.65024411888873,338.48285634988));
#69671=CARTESIAN_POINT('Ctrl Pts',(13.0252559092779,5.4453221312027,332.974283929017));
#69672=CARTESIAN_POINT('Ctrl Pts',(12.747017875004,1.24330839795111,329.324681247404));
#69673=CARTESIAN_POINT('Ctrl Pts',(12.46877984073,-4.0996711035725,330.88323481667));
#69674=CARTESIAN_POINT('Ctrl Pts',(12.1905418064561,-5.68044293934458,336.219683032856));
#69675=CARTESIAN_POINT('Ctrl Pts',(11.9123037721821,-2.04835614241469,340.436846129389));
#69676=CARTESIAN_POINT('Ctrl Pts',(11.6340657379082,3.46347687072457,339.664695786162));
#69677=CARTESIAN_POINT('Ctrl Pts',(11.3558277036343,5.7969282464423,334.611822960457));
#69678=CARTESIAN_POINT('Ctrl Pts',(11.0775896693603,2.81062419710516,329.915174493934));
#69679=CARTESIAN_POINT('Ctrl Pts',(10.7993516350864,-2.75494831436375,329.884795305649));
#69680=CARTESIAN_POINT('Ctrl Pts',(10.5211136008124,-5.79234519187351,334.548564034518));
#69681=CARTESIAN_POINT('Ctrl Pts',(10.2428755665385,-3.51419281376853,339.626608754597));
#69682=CARTESIAN_POINT('Ctrl Pts',(9.96463753226452,1.98888325600979,340.458883156817));
#69683=CARTESIAN_POINT('Ctrl Pts',(9.6863994979906,5.66678897707144,336.281620591485));
#69684=CARTESIAN_POINT('Ctrl Pts',(9.40816146371663,4.1443690044055,330.928234608818));
#69685=CARTESIAN_POINT('Ctrl Pts',(9.12992342944273,-1.18128272534144,329.311445959609));
#69686=CARTESIAN_POINT('Ctrl Pts',(8.85168539516876,-5.42287836274404,332.914962537737));
#69687=CARTESIAN_POINT('Ctrl Pts',(8.57344736089482,-4.68799815077282,338.431881276968));
#69688=CARTESIAN_POINT('Ctrl Pts',(8.2952093266209,0.349025745286411,340.799424444239));
#69689=CARTESIAN_POINT('Ctrl Pts',(8.01697129234695,5.06568404854495,337.844900210057));
#69690=CARTESIAN_POINT('Ctrl Pts',(7.73873325807302,5.13377070045174,332.279693051656));
#69691=CARTESIAN_POINT('Ctrl Pts',(7.46049522379906,0.490422830949281,329.210795885065));
#69692=CARTESIAN_POINT('Ctrl Pts',(7.18225718952515,-4.60250880545255,331.454708526691));
#69693=CARTESIAN_POINT('Ctrl Pts',(6.90401915525119,-5.47267361015814,336.951813491864));
#69694=CARTESIAN_POINT('Ctrl Pts',(6.62578112097724,-1.31897021806641,340.658276570979));
#69695=CARTESIAN_POINT('Ctrl Pts',(6.34754308670334,4.04196323422092,339.17126259052));
#69696=CARTESIAN_POINT('Ctrl Pts',(6.06930505242936,5.69966438415706,333.858154886264));
#69697=CARTESIAN_POINT('Ctrl Pts',(5.79106701815547,2.11523392583091,329.589484673758));
#69698=CARTESIAN_POINT('Ctrl Pts',(5.55920198959383,-2.46923262374946,330.175198721871));
#69699=CARTESIAN_POINT('Ctrl Pts',(5.37370996674454,-4.61534172680647,332.799716245588));
#69700=CARTESIAN_POINT('Ctrl Pts',(5.28096395531991,-4.94983430610851,334.445130104656));
#69701=CARTESIAN_POINT('Ctrl Pts',(5.23459094960758,-4.90621187798767,335.262000892055));
#69702=CARTESIAN_POINT('Ctrl Pts',(185.617269906516,-2.29216991494913,330.278048508348));
#69703=CARTESIAN_POINT('Ctrl Pts',(185.570895172505,-3.07839177256439,330.659702437128));
#69704=CARTESIAN_POINT('Ctrl Pts',(185.478147432782,-4.44361545955773,331.823307916884));
#69705=CARTESIAN_POINT('Ctrl Pts',(185.292653681635,-5.78724472188837,335.186795932361));
#69706=CARTESIAN_POINT('Ctrl Pts',(185.060788653073,-3.96398626270871,339.775335086267));
#69707=CARTESIAN_POINT('Ctrl Pts',(184.782550618799,1.88008622527413,340.918642604601));
#69708=CARTESIAN_POINT('Ctrl Pts',(184.504312584525,5.9896209117165,336.621390747211));
#69709=CARTESIAN_POINT('Ctrl Pts',(184.226074550251,4.6073751195171,330.840900737945));
#69710=CARTESIAN_POINT('Ctrl Pts',(183.947836515977,-1.00552743017874,328.874688417676));
#69711=CARTESIAN_POINT('Ctrl Pts',(183.669598481703,-5.69432997152738,332.530888270267));
#69712=CARTESIAN_POINT('Ctrl Pts',(183.391360447429,-5.15824071662504,338.45226508174));
#69713=CARTESIAN_POINT('Ctrl Pts',(183.113122413155,0.111866319196326,341.205914807967));
#69714=CARTESIAN_POINT('Ctrl Pts',(182.834884378881,5.27911593835755,338.264294481376));
#69715=CARTESIAN_POINT('Ctrl Pts',(182.556646344607,5.60190435506298,332.327181838327));
#69716=CARTESIAN_POINT('Ctrl Pts',(182.278408310334,0.783851916427845,328.842820661638));
#69717=CARTESIAN_POINT('Ctrl Pts',(182.000170276059,-4.75350024470837,331.008840846666));
#69718=CARTESIAN_POINT('Ctrl Pts',(181.721932241786,-5.9286510752286,336.837473644445));
#69719=CARTESIAN_POINT('Ctrl Pts',(181.443694207511,-1.66315801529447,340.979892067162));
#69720=CARTESIAN_POINT('Ctrl Pts',(181.165456173238,4.12858620849688,339.634647530392));
#69721=CARTESIAN_POINT('Ctrl Pts',(180.887218138964,6.13159013610263,334.036257625006));
#69722=CARTESIAN_POINT('Ctrl Pts',(180.60898010469,2.50772306420635,329.322278673983));
#69723=CARTESIAN_POINT('Ctrl Pts',(180.330742070416,-3.41744379639589,329.818661415471));
#69724=CARTESIAN_POINT('Ctrl Pts',(180.052504036142,-6.20647327246837,335.069881763432));
#69725=CARTESIAN_POINT('Ctrl Pts',(179.774266001868,-3.29991365053048,340.256972826555));
#69726=CARTESIAN_POINT('Ctrl Pts',(179.496027967594,2.63492792479757,340.619817425265));
#69727=CARTESIAN_POINT('Ctrl Pts',(179.21778993332,6.15173508641257,335.825438571107));
#69728=CARTESIAN_POINT('Ctrl Pts',(178.939551899046,4.02318573146549,330.273566897255));
#69729=CARTESIAN_POINT('Ctrl Pts',(178.661313864772,-1.79738177270635,329.059073133759));
#69730=CARTESIAN_POINT('Ctrl Pts',(178.383075830499,-5.96851856101238,333.296480260058));
#69731=CARTESIAN_POINT('Ctrl Pts',(178.104837796224,-4.66243395702323,339.09718231172));
#69732=CARTESIAN_POINT('Ctrl Pts',(177.826599761951,0.922297469772181,341.137960628148));
#69733=CARTESIAN_POINT('Ctrl Pts',(177.548361727676,5.66065012278018,337.546023073378));
#69734=CARTESIAN_POINT('Ctrl Pts',(177.270123693403,5.204307708571,331.617637722823));
#69735=CARTESIAN_POINT('Ctrl Pts',(176.991885659128,-0.02795107401978,328.793196310758));
#69736=CARTESIAN_POINT('Ctrl Pts',(176.713647624855,-5.23455956870826,331.664647031874));
#69737=CARTESIAN_POINT('Ctrl Pts',(176.43540959058,-5.63749000907656,337.596901942197));
#69738=CARTESIAN_POINT('Ctrl Pts',(176.157171556307,-0.866979077378676,
341.14601827033));
#69739=CARTESIAN_POINT('Ctrl Pts',(175.878933522033,4.69914575706443,339.055024346885));
#69740=CARTESIAN_POINT('Ctrl Pts',(175.600695487759,5.95293388951394,333.242794432354));
#69741=CARTESIAN_POINT('Ctrl Pts',(175.322457453485,1.74380245672373,329.043126130946));
#69742=CARTESIAN_POINT('Ctrl Pts',(175.044219419211,-4.06559075212348,330.309993055851));
#69743=CARTESIAN_POINT('Ctrl Pts',(174.765981384937,-6.14405133576617,335.880810129014));
#69744=CARTESIAN_POINT('Ctrl Pts',(174.487743350663,-2.58420669462633,340.643320747517));
#69745=CARTESIAN_POINT('Ctrl Pts',(174.209505316389,3.34712628734432,340.227039211301));
#69746=CARTESIAN_POINT('Ctrl Pts',(173.931267282115,6.20685087892184,335.013980941847));
#69747=CARTESIAN_POINT('Ctrl Pts',(173.653029247841,3.37064003188176,329.788092568417));
#69748=CARTESIAN_POINT('Ctrl Pts',(173.374791213568,-2.55875742185098,329.345094717325));
#69749=CARTESIAN_POINT('Ctrl Pts',(173.096553179293,-6.14002095674867,334.091519977878));
#69750=CARTESIAN_POINT('Ctrl Pts',(172.818315145019,-4.08667788619891,339.671643945589));
#69751=CARTESIAN_POINT('Ctrl Pts',(172.540077110746,1.71694916124885,340.964669217786));
#69752=CARTESIAN_POINT('Ctrl Pts',(172.261839076472,5.94495730554663,336.784005587194));
#69753=CARTESIAN_POINT('Ctrl Pts',(171.983601042198,4.71736587797027,330.966186361113));
#69754=CARTESIAN_POINT('Ctrl Pts',(171.705363007924,-0.839282587613181,
328.850138372448));
#69755=CARTESIAN_POINT('Ctrl Pts',(171.42712497365,-5.62573381033469,332.377727627579));
#69756=CARTESIAN_POINT('Ctrl Pts',(171.148886939376,-5.24953215100701,338.311737534204));
#69757=CARTESIAN_POINT('Ctrl Pts',(170.870648905102,-0.0559123196677501,
341.206614786856));
#69758=CARTESIAN_POINT('Ctrl Pts',(170.592410870828,5.18901742216613,338.405773259095));
#69759=CARTESIAN_POINT('Ctrl Pts',(170.314172836554,5.67206246544976,332.479503880593));
#69760=CARTESIAN_POINT('Ctrl Pts',(170.03593480228,0.949939503694936,328.86625658841));
#69761=CARTESIAN_POINT('Ctrl Pts',(169.757696768006,-4.64392891951665,330.881855091139));
#69762=CARTESIAN_POINT('Ctrl Pts',(169.479458733732,-5.9761323175663,336.67661439301));
#69763=CARTESIAN_POINT('Ctrl Pts',(169.201220699458,-1.82412729535379,340.932769413205));
#69764=CARTESIAN_POINT('Ctrl Pts',(168.922982665185,4.00185242173016,339.744509510434));
#69765=CARTESIAN_POINT('Ctrl Pts',(168.64474463091,6.15539123863725,334.202283258784));
#69766=CARTESIAN_POINT('Ctrl Pts',(168.366506596637,2.66021836927275,329.392109886269));
#69767=CARTESIAN_POINT('Ctrl Pts',(168.088268562362,-3.27619763281457,329.728214498801));
#69768=CARTESIAN_POINT('Ctrl Pts',(167.810030528089,-6.20609542386578,334.902158854359));
#69769=CARTESIAN_POINT('Ctrl Pts',(167.531792493814,-3.44075104625367,340.165890585137));
#69770=CARTESIAN_POINT('Ctrl Pts',(167.253554459541,2.48211978110324,340.688960774356));
#69771=CARTESIAN_POINT('Ctrl Pts',(166.975316425266,6.12718592136962,335.991355629872));
#69772=CARTESIAN_POINT('Ctrl Pts',(166.697078390993,4.14942397871105,330.383998056239));
#69773=CARTESIAN_POINT('Ctrl Pts',(166.418840356719,-1.63620310381311,329.012677334318));
#69774=CARTESIAN_POINT('Ctrl Pts',(166.140602322445,-5.92031074828621,333.135834249957));
#69775=CARTESIAN_POINT('Ctrl Pts',(165.862364288171,-4.77143660270046,338.969708559367));
#69776=CARTESIAN_POINT('Ctrl Pts',(165.584126253897,0.756114486894692,341.16063991665));
#69777=CARTESIAN_POINT('Ctrl Pts',(165.305888219623,5.5897904720981,337.698042953318));
#69778=CARTESIAN_POINT('Ctrl Pts',(165.027650185349,5.29379824622925,331.759491794775));
#69779=CARTESIAN_POINT('Ctrl Pts',(164.749412151075,0.139765506129893,328.794707186344));
#69780=CARTESIAN_POINT('Ctrl Pts',(164.471174116801,-5.14252797600939,331.524428203033));
#69781=CARTESIAN_POINT('Ctrl Pts',(164.192936082527,-5.70559943815337,337.443630158443));
#69782=CARTESIAN_POINT('Ctrl Pts',(163.914698048254,-1.03272651041366,341.120348785372));
#69783=CARTESIAN_POINT('Ctrl Pts',(163.63646001398,4.58786429291437,339.180513668164));
#69784=CARTESIAN_POINT('Ctrl Pts',(163.358221979706,5.99823975140083,333.404282861963));
#69785=CARTESIAN_POINT('Ctrl Pts',(163.079983945431,1.90411912390037,329.092418120592));
#69786=CARTESIAN_POINT('Ctrl Pts',(162.801745911158,-3.93738351885127,330.201854074189));
#69787=CARTESIAN_POINT('Ctrl Pts',(162.523507876884,-6.16560742203855,335.714477723383));
#69788=CARTESIAN_POINT('Ctrl Pts',(162.24526984261,-2.7357443982375,340.571435711504));
#69789=CARTESIAN_POINT('Ctrl Pts',(161.967031808336,3.20467088030497,340.315569381432));
#69790=CARTESIAN_POINT('Ctrl Pts',(161.688793774062,6.20420699285626,335.181683487698));
#69791=CARTESIAN_POINT('Ctrl Pts',(161.410555739788,3.51023392200846,329.881069338944));
#69792=CARTESIAN_POINT('Ctrl Pts',(161.132317705514,-2.40502900809874,329.278022302551));
#69793=CARTESIAN_POINT('Ctrl Pts',(160.85407967124,-6.1132323156437,333.925949742852));
#69794=CARTESIAN_POINT('Ctrl Pts',(160.575841636966,-4.21141255828351,339.559517251183));
#69795=CARTESIAN_POINT('Ctrl Pts',(160.297603602692,1.55515834346599,341.008883076468));
#69796=CARTESIAN_POINT('Ctrl Pts',(160.019365568419,5.89458338751627,336.943985593446));
#69797=CARTESIAN_POINT('Ctrl Pts',(159.741127534144,4.82463626075106,331.0951212245));
#69798=CARTESIAN_POINT('Ctrl Pts',(159.462889499871,-0.672808350990864,
328.829706471913));
#69799=CARTESIAN_POINT('Ctrl Pts',(159.184651465596,-5.55282666966348,332.22667901667));
#69800=CARTESIAN_POINT('Ctrl Pts',(158.906413431323,-5.33709791317324,338.168687293676));
#69801=CARTESIAN_POINT('Ctrl Pts',(158.628175397049,-0.223593177199989,
341.202838011026));
#69802=CARTESIAN_POINT('Ctrl Pts',(158.349937362775,5.0950997172598,338.544735839393));
#69803=CARTESIAN_POINT('Ctrl Pts',(158.071699328501,5.73809480473883,332.633681908167));
#69804=CARTESIAN_POINT('Ctrl Pts',(157.793461294227,1.11532498404952,328.894163163016));
#69805=CARTESIAN_POINT('Ctrl Pts',(157.515223259953,-4.53096211233226,330.757880761163));
#69806=CARTESIAN_POINT('Ctrl Pts',(157.236985225679,-6.01925215511788,336.514528571211));
#69807=CARTESIAN_POINT('Ctrl Pts',(156.958747191405,-1.98376333916801,340.881315865866));
#69808=CARTESIAN_POINT('Ctrl Pts',(156.680509157131,3.87219581283742,339.850906398494));
#69809=CARTESIAN_POINT('Ctrl Pts',(156.402271122857,6.1746980209185,334.368891728486));
#69810=CARTESIAN_POINT('Ctrl Pts',(156.124033088583,2.8107709935961,329.466035804104));
#69811=CARTESIAN_POINT('Ctrl Pts',(155.845795054309,-3.13255908763759,329.641617141117));
#69812=CARTESIAN_POINT('Ctrl Pts',(155.567557020035,-6.20118593064259,334.734507338127));
#69813=CARTESIAN_POINT('Ctrl Pts',(155.289318985761,-3.5790759744512,340.071036232271));
#69814=CARTESIAN_POINT('Ctrl Pts',(155.011080951487,2.32749917641929,340.753950024433));
#69815=CARTESIAN_POINT('Ctrl Pts',(154.732842917213,6.09816268692131,336.156548807336));
#69816=CARTESIAN_POINT('Ctrl Pts',(154.45460488294,4.27263230836939,330.497799820378));
#69817=CARTESIAN_POINT('Ctrl Pts',(154.176366848666,-1.47382967562362,328.970653485895));
#69818=CARTESIAN_POINT('Ctrl Pts',(153.898128814392,-5.86777991998716,332.976549454396));
#69819=CARTESIAN_POINT('Ctrl Pts',(153.619890780118,-4.87695514006821,338.839336122517));
#69820=CARTESIAN_POINT('Ctrl Pts',(153.341652745844,0.589379388151474,341.178820699513));
#69821=CARTESIAN_POINT('Ctrl Pts',(153.06341471157,5.51484915109007,337.848092719809));
#69822=CARTESIAN_POINT('Ctrl Pts',(152.785176677296,5.37942324711333,331.903712088916));
#69823=CARTESIAN_POINT('Ctrl Pts',(152.506938643022,0.307380029417682,328.80074917289));
#69824=CARTESIAN_POINT('Ctrl Pts',(152.228700608748,-5.04674130435279,331.386747240111));
#69825=CARTESIAN_POINT('Ctrl Pts',(151.950462574474,-5.76954263289824,337.288574033559));
#69826=CARTESIAN_POINT('Ctrl Pts',(151.6722245402,-1.19771984554265,341.090210215707));
#69827=CARTESIAN_POINT('Ctrl Pts',(151.393986505926,4.47323276575143,339.302950374257));
#69828=CARTESIAN_POINT('Ctrl Pts',(151.115748471652,6.0391656927229,333.566936485794));
#69829=CARTESIAN_POINT('Ctrl Pts',(150.837510437378,2.06304540142216,329.146023832335));
#69830=CARTESIAN_POINT('Ctrl Pts',(150.559272403104,-3.8063012042635,330.097218703396));
#69831=CARTESIAN_POINT('Ctrl Pts',(150.281034368831,-6.18266137571024,335.547623605416));
#69832=CARTESIAN_POINT('Ctrl Pts',(150.002796334556,-2.8852844586,340.495482407657));
#69833=CARTESIAN_POINT('Ctrl Pts',(149.724558300283,3.05987541943865,340.400218117578));
#69834=CARTESIAN_POINT('Ctrl Pts',(149.446320266009,6.19703278874562,335.349253368086));
#69835=CARTESIAN_POINT('Ctrl Pts',(149.168082231735,3.64726463587476,329.977783957673));
#69836=CARTESIAN_POINT('Ctrl Pts',(148.889844197461,-2.24954443980059,329.215128081515));
#69837=CARTESIAN_POINT('Ctrl Pts',(148.611606163187,-6.08197978629243,333.761163780382));
#69838=CARTESIAN_POINT('Ctrl Pts',(148.333368128913,-4.33307205277822,339.444061192799));
#69839=CARTESIAN_POINT('Ctrl Pts',(148.055130094639,1.39223194753191,341.048709242821));
#69840=CARTESIAN_POINT('Ctrl Pts',(147.776892060365,5.83990523890187,337.102546099508));
#69841=CARTESIAN_POINT('Ctrl Pts',(147.498654026091,4.92838368939162,331.226907434206));
#69842=CARTESIAN_POINT('Ctrl Pts',(147.220415991817,-0.505842829049313,
328.81378012578));
#69843=CARTESIAN_POINT('Ctrl Pts',(146.942177957543,-5.4758648494996,332.077655487468));
#69844=CARTESIAN_POINT('Ctrl Pts',(146.66393992327,-5.4207665211968,338.023323274573));
#69845=CARTESIAN_POINT('Ctrl Pts',(146.385701888995,-0.391110766774394,
341.194531916781));
#69846=CARTESIAN_POINT('Ctrl Pts',(146.107463854722,4.99746156553142,338.6811100501));
#69847=CARTESIAN_POINT('Ctrl Pts',(145.829225820447,5.79993718156084,332.789587823537));
#69848=CARTESIAN_POINT('Ctrl Pts',(145.550987786174,1.27989605300435,328.926528225684));
#69849=CARTESIAN_POINT('Ctrl Pts',(145.2727497519,-4.41468679215945,330.637004030825));
#69850=CARTESIAN_POINT('Ctrl Pts',(144.994511717626,-6.05797672882878,336.351336839162));
#69851=CARTESIAN_POINT('Ctrl Pts',(144.716273683352,-2.14195083704191,340.825567775901));
#69852=CARTESIAN_POINT('Ctrl Pts',(144.438035649078,3.73971172275569,339.953761149933));
#69853=CARTESIAN_POINT('Ctrl Pts',(144.159797614804,6.18949603263506,334.535961034068));
#69854=CARTESIAN_POINT('Ctrl Pts',(143.88155958053,2.95927119017693,329.544002628035));
#69855=CARTESIAN_POINT('Ctrl Pts',(143.603321546256,-2.98663314473539,329.558932479864));
#69856=CARTESIAN_POINT('Ctrl Pts',(143.325083511982,-6.191748325357,334.567049684898));
#69857=CARTESIAN_POINT('Ctrl Pts',(143.046845477708,-3.71478745785397,339.972479003764));
#69858=CARTESIAN_POINT('Ctrl Pts',(142.768607443434,2.17117902954865,340.814737734546));
#69859=CARTESIAN_POINT('Ctrl Pts',(142.49036940916,6.06468656808442,336.320897471724));
#69860=CARTESIAN_POINT('Ctrl Pts',(142.212131374886,4.39272075771613,330.614889095514));
#69861=CARTESIAN_POINT('Ctrl Pts',(141.933893340612,-1.31038005555615,328.933032272222));
#69862=CARTESIAN_POINT('Ctrl Pts',(141.655655306338,-5.81096443302246,332.818742184414));
#69863=CARTESIAN_POINT('Ctrl Pts',(141.377417272064,-4.97891251999851,338.706160198657));
#69864=CARTESIAN_POINT('Ctrl Pts',(141.099179237791,0.422213923999755,341.192489701428));
#69865=CARTESIAN_POINT('Ctrl Pts',(140.820941203517,5.43588088181075,337.996062806197));
#69866=CARTESIAN_POINT('Ctrl Pts',(140.542703169243,5.46112018785431,332.050193295534));
#69867=CARTESIAN_POINT('Ctrl Pts',(140.264465134969,0.474770103505825,328.811317858483));
#69868=CARTESIAN_POINT('Ctrl Pts',(139.986227100695,-4.94726949723473,331.251704677905));
#69869=CARTESIAN_POINT('Ctrl Pts',(139.707989066421,-5.82927290194103,337.131846789665));
#69870=CARTESIAN_POINT('Ctrl Pts',(139.429751032147,-1.36183860446307,341.055624568556));
#69871=CARTESIAN_POINT('Ctrl Pts',(139.151512997873,4.35533487962575,339.422245061756));
#69872=CARTESIAN_POINT('Ctrl Pts',(138.873274963599,6.07568182931952,333.730636534013));
#69873=CARTESIAN_POINT('Ctrl Pts',(138.595036929325,2.22046524116368,329.203904123231));
#69874=CARTESIAN_POINT('Ctrl Pts',(138.316798895051,-3.67243952479488,329.996163348326));
#69875=CARTESIAN_POINT('Ctrl Pts',(138.038560860777,-6.19520074396771,335.380369612154));
#69876=CARTESIAN_POINT('Ctrl Pts',(137.760322826503,-3.03271768141446,340.415516297154));
#69877=CARTESIAN_POINT('Ctrl Pts',(137.482084792229,2.91284563453323,340.480923609145));
#69878=CARTESIAN_POINT('Ctrl Pts',(137.203846757955,6.18533350520087,335.516568223324));
#69879=CARTESIAN_POINT('Ctrl Pts',(136.925608723682,3.78163211351856,330.078165803492));
#69880=CARTESIAN_POINT('Ctrl Pts',(136.647370689407,-2.09241725194123,329.156457979643));
#69881=CARTESIAN_POINT('Ctrl Pts',(136.369132655134,-6.04628618932257,333.597282417335));
#69882=CARTESIAN_POINT('Ctrl Pts',(136.09089462086,-4.45156753380044,339.325360076563));
#69883=CARTESIAN_POINT('Ctrl Pts',(135.812656586586,1.22828894246125,341.084118635737));
#69884=CARTESIAN_POINT('Ctrl Pts',(135.534418552312,5.78096278574133,337.259571324341));
#69885=CARTESIAN_POINT('Ctrl Pts',(135.256180518038,5.02853240741745,331.361448759813));
#69886=CARTESIAN_POINT('Ctrl Pts',(134.977942483764,-0.338507940176758,
328.802370963477));
#69887=CARTESIAN_POINT('Ctrl Pts',(134.69970444949,-5.39490454743976,331.930765857103));
#69888=CARTESIAN_POINT('Ctrl Pts',(134.421466415216,-5.50047688017788,337.875751621844));
#69889=CARTESIAN_POINT('Ctrl Pts',(134.143228380942,-0.558342766882442,
341.181702569242));
#69890=CARTESIAN_POINT('Ctrl Pts',(133.864990346668,4.89617426245531,338.814796310628));
#69891=CARTESIAN_POINT('Ctrl Pts',(133.586752312394,5.85754443855144,332.947107784052));
#69892=CARTESIAN_POINT('Ctrl Pts',(133.30851427812,1.44353254060325,328.963328143411));
#69893=CARTESIAN_POINT('Ctrl Pts',(133.030276243846,-4.29518786335118,330.519313164433));
#69894=CARTESIAN_POINT('Ctrl Pts',(132.752038209572,-6.09227776197722,336.187158359625));
#69895=CARTESIAN_POINT('Ctrl Pts',(132.473800175299,-2.29857428030914,340.765565850617));
#69896=CARTESIAN_POINT('Ctrl Pts',(132.195562141024,3.60449689149788,340.052998660112));
#69897=CARTESIAN_POINT('Ctrl Pts',(131.917324106751,6.1997744682642,334.703369181358));
#69898=CARTESIAN_POINT('Ctrl Pts',(131.639086072476,3.10561052402562,329.625953426611));
#69899=CARTESIAN_POINT('Ctrl Pts',(131.360848038203,-2.83852635937508,329.480220891463));
#69900=CARTESIAN_POINT('Ctrl Pts',(131.082610003929,-6.17778949935765,334.399908172415));
#69901=CARTESIAN_POINT('Ctrl Pts',(130.804371969655,-3.84778639980326,339.870290866201));
#69902=CARTESIAN_POINT('Ctrl Pts',(130.526133935381,2.01327348561643,340.871279517449));
#69903=CARTESIAN_POINT('Ctrl Pts',(130.247895901107,6.02678200915386,336.484281615479));
#69904=CARTESIAN_POINT('Ctrl Pts',(129.969657866833,4.50960163804743,330.735180382943));
#69905=CARTESIAN_POINT('Ctrl Pts',(129.691419832559,-1.14597359468405,328.899841164347));
#69906=CARTESIAN_POINT('Ctrl Pts',(129.413181798285,-5.74990577411651,332.662527671032));
#69907=CARTESIAN_POINT('Ctrl Pts',(129.134943764011,-5.07723429311236,338.570278032976));
#69908=CARTESIAN_POINT('Ctrl Pts',(128.856705729737,0.254740158825682,341.201636941275));
#69909=CARTESIAN_POINT('Ctrl Pts',(128.578467695463,5.35294332696797,338.141845164577));
#69910=CARTESIAN_POINT('Ctrl Pts',(128.300229661189,5.53882941326574,332.198828453905));
#69911=CARTESIAN_POINT('Ctrl Pts',(128.021991626915,0.641813499997803,328.826405525861));
#69912=CARTESIAN_POINT('Ctrl Pts',(127.743753592642,-4.84418518906642,331.119399124628));
#69913=CARTESIAN_POINT('Ctrl Pts',(127.465515558368,-5.88474663018062,336.97356286915));
#69914=CARTESIAN_POINT('Ctrl Pts',(127.187277524094,-1.52496294749595,341.016617098393));
#69915=CARTESIAN_POINT('Ctrl Pts',(126.90903948982,4.23425672368954,339.538310621564));
#69916=CARTESIAN_POINT('Ctrl Pts',(126.630801455546,6.10776149707195,333.89526347268));
#69917=CARTESIAN_POINT('Ctrl Pts',(126.352563421272,2.37626369500335,329.266016729034));
#69918=CARTESIAN_POINT('Ctrl Pts',(126.074325386998,-3.53589622637518,329.898761799698));
#69919=CARTESIAN_POINT('Ctrl Pts',(125.796087352724,-6.20321637055196,335.212837872628));
#69920=CARTESIAN_POINT('Ctrl Pts',(125.51784931845,-3.17793641079674,340.331595771327));
#69921=CARTESIAN_POINT('Ctrl Pts',(125.239611284176,2.76368888688211,340.557626924905));
#69922=CARTESIAN_POINT('Ctrl Pts',(124.961373249902,6.16911768505035,335.683505879936));
#69923=CARTESIAN_POINT('Ctrl Pts',(124.683135215628,3.91323823967566,330.182141577479));
#69924=CARTESIAN_POINT('Ctrl Pts',(124.404897181354,-1.93376217894764,329.102054837896));
#69925=CARTESIAN_POINT('Ctrl Pts',(124.12665914708,-6.00617758823367,333.434425320048));
#69926=CARTESIAN_POINT('Ctrl Pts',(123.848421112806,-4.56681247583354,339.203500578147));
#69927=CARTESIAN_POINT('Ctrl Pts',(123.570183078532,1.06344903959737,341.115085399248));
#69928=CARTESIAN_POINT('Ctrl Pts',(123.291945044258,5.71779906787188,337.414946607972));
#69929=CARTESIAN_POINT('Ctrl Pts',(123.013707009985,5.12500928613626,331.498646959113));
#69930=CARTESIAN_POINT('Ctrl Pts',(122.73546897571,-0.170925872473485,328.795487315991));
#69931=CARTESIAN_POINT('Ctrl Pts',(122.457230941437,-5.31000488077602,331.786117384526));
#69932=CARTESIAN_POINT('Ctrl Pts',(122.178992907162,-5.5761707855341,337.726080092452));
#69933=CARTESIAN_POINT('Ctrl Pts',(121.900754872889,-0.725167064553412,
341.164359336411));
#69934=CARTESIAN_POINT('Ctrl Pts',(121.622516838615,4.79131176811961,338.94569700314));
#69935=CARTESIAN_POINT('Ctrl Pts',(121.344278804341,5.91087451083504,333.106126768479));
#69936=CARTESIAN_POINT('Ctrl Pts',(121.066040770067,1.60611495932192,329.004536044862));
#69937=CARTESIAN_POINT('Ctrl Pts',(120.787802735793,-4.17255258414297,330.404894099973));
#69938=CARTESIAN_POINT('Ctrl Pts',(120.509564701519,-6.12213020791506,336.022113015885));
#69939=CARTESIAN_POINT('Ctrl Pts',(120.231326667245,-2.45351930237723,340.701353903483));
#69940=CARTESIAN_POINT('Ctrl Pts',(119.953088632971,3.46665005306664,340.148546465701));
#69941=CARTESIAN_POINT('Ctrl Pts',(119.674850598697,6.20552582248217,334.870993928765));
#69942=CARTESIAN_POINT('Ctrl Pts',(119.396612564423,3.24968213801681,329.711828359275));
#69943=CARTESIAN_POINT('Ctrl Pts',(119.118374530149,-2.68834687927684,329.405539851193));
#69944=CARTESIAN_POINT('Ctrl Pts',(118.840136495875,-6.15931964539302,334.233204847575));
#69945=CARTESIAN_POINT('Ctrl Pts',(118.561898461601,-3.97797568434098,339.764546437459));
#69946=CARTESIAN_POINT('Ctrl Pts',(118.283660427328,1.85389784740593,340.923534086277));
#69947=CARTESIAN_POINT('Ctrl Pts',(118.005422393054,5.98447668807579,336.646581935339));
#69948=CARTESIAN_POINT('Ctrl Pts',(117.72718435878,4.62318960282962,330.85858584585));
#69949=CARTESIAN_POINT('Ctrl Pts',(117.448946324506,-0.980730342766608,
328.871104398451));
#69950=CARTESIAN_POINT('Ctrl Pts',(117.170708290232,-5.68464852836201,332.508019982243));
#69951=CARTESIAN_POINT('Ctrl Pts',(116.892470255958,-5.17184866475443,338.431788846766));
#69952=CARTESIAN_POINT('Ctrl Pts',(116.614232221684,0.087080382136921,341.206255739731));
#69953=CARTESIAN_POINT('Ctrl Pts',(116.33599418741,5.26609704764564,338.285333344531));
#69954=CARTESIAN_POINT('Ctrl Pts',(116.057756153136,5.61249417999503,332.349509030494));
#69955=CARTESIAN_POINT('Ctrl Pts',(115.779518118862,0.80838824364127,328.846001157991));
#69956=CARTESIAN_POINT('Ctrl Pts',(115.501280084588,-4.73756365211115,330.989927189924));
#69957=CARTESIAN_POINT('Ctrl Pts',(115.223042050314,-5.93592331064607,336.813837851088));
#69958=CARTESIAN_POINT('Ctrl Pts',(114.94480401604,-1.68697376108552,340.973216288509));
#69959=CARTESIAN_POINT('Ctrl Pts',(114.666565981766,4.1100867093313,339.651062302496));
#69960=CARTESIAN_POINT('Ctrl Pts',(114.388327947492,6.13538127137518,334.060697091047));
#69961=CARTESIAN_POINT('Ctrl Pts',(114.110089913219,2.53032699875718,329.332316295059));
#69962=CARTESIAN_POINT('Ctrl Pts',(113.831851878945,-3.39677101305501,329.805085180218));
#69963=CARTESIAN_POINT('Ctrl Pts',(113.553613844671,-6.20670240244458,335.045150718677));
#69964=CARTESIAN_POINT('Ctrl Pts',(113.275375810397,-3.32083460788806,340.243782109027));
#69965=CARTESIAN_POINT('Ctrl Pts',(112.997137776123,2.61251409088887,340.630272056021));
#69966=CARTESIAN_POINT('Ctrl Pts',(112.718899741849,6.14839716910185,335.849944439884));
#69967=CARTESIAN_POINT('Ctrl Pts',(112.440661707575,4.04198691542352,330.289635356424));
#69968=CARTESIAN_POINT('Ctrl Pts',(112.162423673301,-1.77369507090989,329.051958381506));
#69969=CARTESIAN_POINT('Ctrl Pts',(111.884185639027,-5.96168327036564,333.27271140693));
#69970=CARTESIAN_POINT('Ctrl Pts',(111.605947604753,-4.67872272690766,339.078571679476));
#69971=CARTESIAN_POINT('Ctrl Pts',(111.327709570479,0.897832605199222,341.141586921387));
#69972=CARTESIAN_POINT('Ctrl Pts',(111.049471536205,5.65046020750232,337.568558495216));
#69973=CARTESIAN_POINT('Ctrl Pts',(110.771233501931,5.21774387803648,331.638401849845));
#69974=CARTESIAN_POINT('Ctrl Pts',(110.492995467657,-0.00321899453002624,
328.793134209766));
#69975=CARTESIAN_POINT('Ctrl Pts',(110.214757433383,-5.22122784332861,331.643815692195));
#69976=CARTESIAN_POINT('Ctrl Pts',(109.93651939911,-5.64779296550117,337.574417976698));
#69977=CARTESIAN_POINT('Ctrl Pts',(109.658281364835,-0.891461844520826,
341.142514882332));
#69978=CARTESIAN_POINT('Ctrl Pts',(109.380043330562,4.68295065322101,339.073716543821));
#69979=CARTESIAN_POINT('Ctrl Pts',(109.101805296288,5.95988845674028,333.266528661003));
#69980=CARTESIAN_POINT('Ctrl Pts',(108.823567262014,1.76752459131841,329.050121839987));
#69981=CARTESIAN_POINT('Ctrl Pts',(108.54532922774,-4.04687050293616,330.293830386358));
#69982=CARTESIAN_POINT('Ctrl Pts',(108.267091193466,-6.14751226835692,335.856321324217));
#69983=CARTESIAN_POINT('Ctrl Pts',(107.988853159192,-2.60667276223889,340.632978822125));
#69984=CARTESIAN_POINT('Ctrl Pts',(107.710615124918,3.32627186335888,340.2403347976));
#69985=CARTESIAN_POINT('Ctrl Pts',(107.432377090644,6.20674589564442,335.038712876532));
#69986=CARTESIAN_POINT('Ctrl Pts',(107.15413905637,3.39138083091633,329.801564720073));
#69987=CARTESIAN_POINT('Ctrl Pts',(106.875901022096,-2.53620436564467,329.334943891222));
#69988=CARTESIAN_POINT('Ctrl Pts',(106.597662987822,-6.13635225016862,334.067061437308));
#69989=CARTESIAN_POINT('Ctrl Pts',(106.319424953548,-4.10526024712359,339.655322932224));
#69990=CARTESIAN_POINT('Ctrl Pts',(106.041186919274,1.69316849116485,340.971463284693));
#69991=CARTESIAN_POINT('Ctrl Pts',(105.762948885,5.93780149623726,336.807679919453));
#69992=CARTESIAN_POINT('Ctrl Pts',(105.484710850726,4.73340171001917,330.985015373441));
#69993=CARTESIAN_POINT('Ctrl Pts',(105.206472816452,-0.814770960588805,
328.846842958148));
#69994=CARTESIAN_POINT('Ctrl Pts',(104.928234782179,-5.61524034666409,332.355331939712));
#69995=CARTESIAN_POINT('Ctrl Pts',(104.649996747905,-5.26268654741741,338.290793764967));
#69996=CARTESIAN_POINT('Ctrl Pts',(104.371758713631,-0.0806429807318726,
341.206342724146));
#69997=CARTESIAN_POINT('Ctrl Pts',(104.093520679357,5.17540545908285,338.426422570846));
#69998=CARTESIAN_POINT('Ctrl Pts',(103.815282645083,5.68206069795661,332.502124998195));
#69999=CARTESIAN_POINT('Ctrl Pts',(103.537044610809,0.974372701394095,328.870090446125));
#70000=CARTESIAN_POINT('Ctrl Pts',(103.258806576535,-4.62748274152016,330.86338341433));
#70001=CARTESIAN_POINT('Ctrl Pts',(102.980568542261,-5.98276557407492,336.652788366844));
#70002=CARTESIAN_POINT('Ctrl Pts',(102.702330507987,-1.84775274477625,340.925453830221));
#70003=CARTESIAN_POINT('Ctrl Pts',(102.424092473713,3.98291550561775,339.76041777316));
#70004=CARTESIAN_POINT('Ctrl Pts',(102.145854439439,6.15852098424286,334.226816589321));
#70005=CARTESIAN_POINT('Ctrl Pts',(101.867616405165,2.682542655249,329.402754409294));
#70006=CARTESIAN_POINT('Ctrl Pts',(101.589378370891,-3.25516547420216,329.715201892649));
#70007=CARTESIAN_POINT('Ctrl Pts',(101.311140336617,-6.20565629414165,334.877430595626));
#70008=CARTESIAN_POINT('Ctrl Pts',(101.032902302343,-3.4613079282841,340.152139431878));
#70009=CARTESIAN_POINT('Ctrl Pts',(100.75466426807,2.4594316345385,340.698805956947));
#70010=CARTESIAN_POINT('Ctrl Pts',(100.476426233796,6.12318708749654,336.015762369565));
#70011=CARTESIAN_POINT('Ctrl Pts',(100.198188199522,4.16778412835227,330.400568648261));
#70012=CARTESIAN_POINT('Ctrl Pts',(99.9199501652471,-1.61233280898796,329.006205190952));
#70013=CARTESIAN_POINT('Ctrl Pts',(99.6417121309733,-5.91283572551321,333.112258761641));
#70014=CARTESIAN_POINT('Ctrl Pts',(99.3634740966994,-4.78721657004721,338.950664603756));
#70015=CARTESIAN_POINT('Ctrl Pts',(99.0852360624254,0.73156057255035,341.163603850719));
#70016=CARTESIAN_POINT('Ctrl Pts',(98.8069980281515,5.5789953755348,337.720294818521));
#70017=CARTESIAN_POINT('Ctrl Pts',(98.5287599938776,5.30666846822774,331.780611382852));
#70018=CARTESIAN_POINT('Ctrl Pts',(98.2505219596036,0.164490233926267,328.795313363042));
#70019=CARTESIAN_POINT('Ctrl Pts',(97.9722839253297,-5.12863826017746,331.503964688944));
#70020=CARTESIAN_POINT('Ctrl Pts',(97.6940458910556,-5.71529112149298,337.420876018406));
#70021=CARTESIAN_POINT('Ctrl Pts',(97.4158078567819,-1.05710567817306,341.116185157848));
#70022=CARTESIAN_POINT('Ctrl Pts',(97.1375698225077,4.57117004315204,339.198761452678));
#70023=CARTESIAN_POINT('Ctrl Pts',(96.8593317882339,6.00455048623575,333.428196336003));
#70024=CARTESIAN_POINT('Ctrl Pts',(96.5810937539601,1.92764357512081,329.100052241994));
#70025=CARTESIAN_POINT('Ctrl Pts',(96.3028557196859,-3.91823339290997,330.18620312242));
#70026=CARTESIAN_POINT('Ctrl Pts',(96.0246176854122,-6.16840540929736,335.689904345876));
#70027=CARTESIAN_POINT('Ctrl Pts',(95.7463796511382,-2.75792282708715,340.560490534093));
#70028=CARTESIAN_POINT('Ctrl Pts',(95.4681416168641,3.18346482666672,340.328296631878));
#70029=CARTESIAN_POINT('Ctrl Pts',(95.1899035825903,6.20343379685237,335.206403556118));
#70030=CARTESIAN_POINT('Ctrl Pts',(94.9116655483162,3.53060313419934,329.89509698342));
#70031=CARTESIAN_POINT('Ctrl Pts',(94.6334275140424,-2.38220991309158,329.268484560793));
#70032=CARTESIAN_POINT('Ctrl Pts',(94.3551894797685,-6.10890408449904,333.901599259696));
#70033=CARTESIAN_POINT('Ctrl Pts',(94.0769514454943,-4.22954714483822,339.542700105609));
#70034=CARTESIAN_POINT('Ctrl Pts',(93.7987134112207,1.53120278162712,341.015032114749));
#70035=CARTESIAN_POINT('Ctrl Pts',(93.5204753769465,5.88679051590925,336.967457933911));
#70036=CARTESIAN_POINT('Ctrl Pts',(93.2422373426728,4.84015748262706,331.114376646755));
#70037=CARTESIAN_POINT('Ctrl Pts',(92.9639993083986,-0.648216631854655,
328.827074559167));
#70038=CARTESIAN_POINT('Ctrl Pts',(92.6857612741249,-5.54173191094504,332.204575036399));
#70039=CARTESIAN_POINT('Ctrl Pts',(92.4075232398509,-5.34968161119029,338.147395742324));
#70040=CARTESIAN_POINT('Ctrl Pts',(92.1292852055768,-0.248307458017522,
341.201897831003));
#70041=CARTESIAN_POINT('Ctrl Pts',(91.8510471713032,5.08093478436595,338.565009820033));
#70042=CARTESIAN_POINT('Ctrl Pts',(91.5728091370289,5.74747816961128,332.656564916677));
#70043=CARTESIAN_POINT('Ctrl Pts',(91.2945711027553,1.13964567124306,328.898655800242));
#70044=CARTESIAN_POINT('Ctrl Pts',(91.0163330684812,-4.51402283848238,330.739860200232));
#70045=CARTESIAN_POINT('Ctrl Pts',(90.7380950342073,-6.02523921620042,336.490532014909));
#70046=CARTESIAN_POINT('Ctrl Pts',(90.4598569999334,-2.00718249759639,340.873364599721));
#70047=CARTESIAN_POINT('Ctrl Pts',(90.1816189656593,3.85283597308675,339.866297182088));
#70048=CARTESIAN_POINT('Ctrl Pts',(89.9033809313856,6.17716373903393,334.393500666882));
#70049=CARTESIAN_POINT('Ctrl Pts',(89.6251428971114,2.832799516457,329.477279637762));
#70050=CARTESIAN_POINT('Ctrl Pts',(89.3469048628377,-3.11118301032018,329.62917756985));
#70051=CARTESIAN_POINT('Ctrl Pts',(89.0686668285635,-6.20007880951249,334.709799972876));
#70052=CARTESIAN_POINT('Ctrl Pts',(88.7904287942898,-3.59925379822841,340.056734657449));
#70053=CARTESIAN_POINT('Ctrl Pts',(88.5121907600156,2.30455329879092,340.763178584161));
#70054=CARTESIAN_POINT('Ctrl Pts',(88.2339527257419,6.09350584866075,336.180838588566));
#70055=CARTESIAN_POINT('Ctrl Pts',(87.9557146914679,4.2905380212135,330.514860449392));
#70056=CARTESIAN_POINT('Ctrl Pts',(87.677476657194,-1.44979322006398,328.96482867526));
#70057=CARTESIAN_POINT('Ctrl Pts',(87.39923862292,-5.8596706222016,332.953184546859));
#70058=CARTESIAN_POINT('Ctrl Pts',(87.1210005886461,-4.89221478294142,338.819872748859));
#70059=CARTESIAN_POINT('Ctrl Pts',(86.8427625543722,0.564754353652266,341.18112011046));
#70060=CARTESIAN_POINT('Ctrl Pts',(86.5645245200982,5.50345675565987,337.870044779876));
#70061=CARTESIAN_POINT('Ctrl Pts',(86.2862864858242,5.39171812388697,331.92517171659));
#70062=CARTESIAN_POINT('Ctrl Pts',(86.0080484515503,0.332079351452054,328.802023184599));
#70063=CARTESIAN_POINT('Ctrl Pts',(85.7298104172765,-5.03230374032721,331.366666494113));
#70064=CARTESIAN_POINT('Ctrl Pts',(85.4515723830023,-5.77861596628966,337.265566334065));
#70065=CARTESIAN_POINT('Ctrl Pts',(85.1733343487285,-1.22197761221993,341.08538938895));
#70066=CARTESIAN_POINT('Ctrl Pts',(84.8950963144546,4.45605156022403,339.320740421795));
#70067=CARTESIAN_POINT('Ctrl Pts',(84.6168582801807,6.04482798706362,333.591011743583));
#70068=CARTESIAN_POINT('Ctrl Pts',(84.3386202459067,2.08635499168976,329.154290791653));
#70069=CARTESIAN_POINT('Ctrl Pts',(84.0603822116327,-3.78673518500859,330.082090897696));
#70070=CARTESIAN_POINT('Ctrl Pts',(83.7821441773588,-6.18479437454427,335.522983598705));
#70071=CARTESIAN_POINT('Ctrl Pts',(83.5039061430849,-2.907159053976,340.483941970407));
#70072=CARTESIAN_POINT('Ctrl Pts',(83.225668108811,3.03833322082874,340.412367738718));
#70073=CARTESIAN_POINT('Ctrl Pts',(82.947430074537,6.19559194460378,335.373943519624));
#70074=CARTESIAN_POINT('Ctrl Pts',(82.6691920402631,3.66724738760314,329.992356851969));
#70075=CARTESIAN_POINT('Ctrl Pts',(82.3909540059891,-2.2264759685182,329.206210388569));
#70076=CARTESIAN_POINT('Ctrl Pts',(82.1127159717152,-6.07699519106181,333.736939135386));
#70077=CARTESIAN_POINT('Ctrl Pts',(81.8344779374412,-4.35074562306998,339.42676019491));
#70078=CARTESIAN_POINT('Ctrl Pts',(81.5562399031674,1.36811898631292,341.054208762439));
#70079=CARTESIAN_POINT('Ctrl Pts',(81.2780018688933,5.83148099535957,337.125799308652));
#70080=CARTESIAN_POINT('Ctrl Pts',(80.9997638346196,4.9433789674834,331.246575206061));
#70081=CARTESIAN_POINT('Ctrl Pts',(80.7215258003455,-0.481188974698351,
328.811813636409));
#70082=CARTESIAN_POINT('Ctrl Pts',(80.4432877660716,-5.46417689713705,332.055859355143));
#70083=CARTESIAN_POINT('Ctrl Pts',(80.1650497317976,-5.43277033219188,338.001699488218));
#70084=CARTESIAN_POINT('Ctrl Pts',(79.8868116975237,-0.415790620952878,
341.192924305967));
#70085=CARTESIAN_POINT('Ctrl Pts',(79.6085736632497,4.98275400607507,338.700993895544));
#70086=CARTESIAN_POINT('Ctrl Pts',(79.3303356289758,5.8086988270565,332.81271601376));
#70087=CARTESIAN_POINT('Ctrl Pts',(79.0520975947017,1.30408647070233,328.931676361891));
#70088=CARTESIAN_POINT('Ctrl Pts',(78.7738595604281,-4.39726679153062,330.619447744404));
#70089=CARTESIAN_POINT('Ctrl Pts',(78.4956215261539,-6.06331322272737,336.327187275032));
#70090=CARTESIAN_POINT('Ctrl Pts',(78.21738349188,-2.16514660378369,340.816986632616));
#70091=CARTESIAN_POINT('Ctrl Pts',(77.939145457606,3.71994309594081,339.96862321603));
#70092=CARTESIAN_POINT('Ctrl Pts',(77.6609074233321,6.1912959227905,334.560627610852));
#70093=CARTESIAN_POINT('Ctrl Pts',(77.3826693890583,2.98098786467339,329.555837562069));
#70094=CARTESIAN_POINT('Ctrl Pts',(77.1044313547843,-2.96492875754574,329.54707502687));
#70095=CARTESIAN_POINT('Ctrl Pts',(76.8261933205103,-6.18997402124187,334.542381254471));
#70096=CARTESIAN_POINT('Ctrl Pts',(76.5479552862364,-3.73457148951113,339.957637450403));
#70097=CARTESIAN_POINT('Ctrl Pts',(76.2697172519624,2.14799217595916,340.823342932708));
#70098=CARTESIAN_POINT('Ctrl Pts',(75.9914792176885,6.05937512586425,336.345052558068));
#70099=CARTESIAN_POINT('Ctrl Pts',(75.7132411834145,4.41015895899399,330.632427303832));
#70100=CARTESIAN_POINT('Ctrl Pts',(75.4350031491406,-1.28619499070553,328.927859047602));
#70101=CARTESIAN_POINT('Ctrl Pts',(75.1567651148666,-5.80222678164153,332.795604918733));
#70102=CARTESIAN_POINT('Ctrl Pts',(74.8785270805928,-4.99364069579202,338.686291619127));
#70103=CARTESIAN_POINT('Ctrl Pts',(74.6002890463187,0.397535750569984,341.194122910221));
#70104=CARTESIAN_POINT('Ctrl Pts',(74.3220510120449,5.42389950625196,338.017699031711));
#70105=CARTESIAN_POINT('Ctrl Pts',(74.0438129777708,5.47283074167201,332.071977292964));
#70106=CARTESIAN_POINT('Ctrl Pts',(73.7655749434971,0.499425984308978,328.81325877492));
#70107=CARTESIAN_POINT('Ctrl Pts',(73.4873369092229,-4.93229462733895,331.232021362981));
#70108=CARTESIAN_POINT('Ctrl Pts',(73.2090988749492,-5.83772126002729,337.108602330961));
#70109=CARTESIAN_POINT('Ctrl Pts',(72.9308608406751,-1.38595725701314,341.050150062737));
#70110=CARTESIAN_POINT('Ctrl Pts',(72.6526228064015,4.33767926406639,339.439564382009));
#70111=CARTESIAN_POINT('Ctrl Pts',(72.3743847721271,6.08069154855318,333.754855995773));
#70112=CARTESIAN_POINT('Ctrl Pts',(72.0961467378534,2.24354294979286,329.212797883922));
#70113=CARTESIAN_POINT('Ctrl Pts',(71.8179087035794,-3.65247189935271,329.981569735032));
#70114=CARTESIAN_POINT('Ctrl Pts',(71.5396706693055,-6.19666719685916,335.355680968395));
#70115=CARTESIAN_POINT('Ctrl Pts',(71.2614326350313,-3.05427247046587,340.403389026903));
#70116=CARTESIAN_POINT('Ctrl Pts',(70.9831946007578,2.89098302108621,340.492486729315));
#70117=CARTESIAN_POINT('Ctrl Pts',(70.7049565664835,6.18322606502682,335.541210429205));
#70118=CARTESIAN_POINT('Ctrl Pts',(70.4267185322099,3.8012138133597,330.093273306468));
#70119=CARTESIAN_POINT('Ctrl Pts',(70.1484804979358,-2.06911624900363,329.148166847215));
#70120=CARTESIAN_POINT('Ctrl Pts',(69.8702424636618,-6.04064886976221,333.57320129936));
#70121=CARTESIAN_POINT('Ctrl Pts',(69.592004429388,-4.46876718257118,339.307587859566));
#70122=CARTESIAN_POINT('Ctrl Pts',(69.313766395114,1.20403618916992,341.088964620942));
#70123=CARTESIAN_POINT('Ctrl Pts',(69.0355283608399,5.7719133216548,337.282588422648));
#70124=CARTESIAN_POINT('Ctrl Pts',(68.7572903265662,5.04299079215806,331.381514519843));
#70125=CARTESIAN_POINT('Ctrl Pts',(68.479052292292,-0.313809952880065,328.801071333416));
#70126=CARTESIAN_POINT('Ctrl Pts',(68.2008142580184,-5.38263193598747,331.90929348828));
#70127=CARTESIAN_POINT('Ctrl Pts',(67.9225762237442,-5.51189203895631,337.853811390193));
#70128=CARTESIAN_POINT('Ctrl Pts',(67.6443381894704,-0.582970173168094,
341.179428701516));
#70129=CARTESIAN_POINT('Ctrl Pts',(67.3661001551964,4.88093481591085,338.834275501673));
#70130=CARTESIAN_POINT('Ctrl Pts',(67.0878621209226,5.86567796690818,332.97046426776));
#70131=CARTESIAN_POINT('Ctrl Pts',(66.8096240866486,1.46757502493876,328.969128019425));
#70132=CARTESIAN_POINT('Ctrl Pts',(66.5313860523745,-4.2772998560451,330.502233972139));
#70133=CARTESIAN_POINT('Ctrl Pts',(66.2531480181009,-6.09695979197876,336.162873421702));
#70134=CARTESIAN_POINT('Ctrl Pts',(65.9749099838266,-2.32152971779252,340.756361096154));
#70135=CARTESIAN_POINT('Ctrl Pts',(65.696671949553,3.58433391268944,340.067321156415));
#70136=CARTESIAN_POINT('Ctrl Pts',(65.4184339152789,6.20090721617813,334.728075384972));
#70137=CARTESIAN_POINT('Ctrl Pts',(65.1401958810049,3.12699949262064,329.63837081914));
#70138=CARTESIAN_POINT('Ctrl Pts',(64.8619578467309,-2.81650951087796,329.468954215065));
#70139=CARTESIAN_POINT('Ctrl Pts',(64.583719812457,-6.17534930785609,334.375296689724));
#70140=CARTESIAN_POINT('Ctrl Pts',(64.305481778183,-3.86716219302106,339.854920171618));
#70141=CARTESIAN_POINT('Ctrl Pts',(64.0272437439093,1.98986258712899,340.879255070521));
#70142=CARTESIAN_POINT('Ctrl Pts',(63.749005709635,6.02081984139441,336.508284368871));
#70143=CARTESIAN_POINT('Ctrl Pts',(63.4707676753615,4.52655959436737,330.753183364147));
#70144=CARTESIAN_POINT('Ctrl Pts',(63.1925296410872,-1.12165758050052,328.895323303236));
#70145=CARTESIAN_POINT('Ctrl Pts',(62.9142916068136,-5.74054614938183,332.639634942063));
#70146=CARTESIAN_POINT('Ctrl Pts',(62.6360535725393,-5.09142024729771,338.550018755629));
#70147=CARTESIAN_POINT('Ctrl Pts',(62.3578155382655,0.230026866491849,341.202602755343));
#70148=CARTESIAN_POINT('Ctrl Pts',(62.0795775039915,5.34038172009283,338.163149756747));
#70149=CARTESIAN_POINT('Ctrl Pts',(61.8013394697177,5.5499470930696,332.220920914397));
#70150=CARTESIAN_POINT('Ctrl Pts',(61.5231014354438,0.666407935821213,328.829011929764));
#70151=CARTESIAN_POINT('Ctrl Pts',(61.2448634011698,-4.82868394796529,331.100127613554));
#70152=CARTESIAN_POINT('Ctrl Pts',(60.9666253668957,-5.89256384396229,336.950098624361));
#70153=CARTESIAN_POINT('Ctrl Pts',(60.6883873326221,-1.54892487445486,341.010492911002));
#70154=CARTESIAN_POINT('Ctrl Pts',(60.4101492983478,4.21613959024611,339.555146567945));
#70155=CARTESIAN_POINT('Ctrl Pts',(60.1319112640742,6.11211498309658,333.919609453339));
#70156=CARTESIAN_POINT('Ctrl Pts',(59.8536732298,2.39909267062866,329.275530796865));
#70157=CARTESIAN_POINT('Ctrl Pts',(59.5754351955263,-3.51554157512524,329.884713035079));
#70158=CARTESIAN_POINT('Ctrl Pts',(59.2971971612521,-6.20401520669551,335.188118619492));
#70159=CARTESIAN_POINT('Ctrl Pts',(59.0189591269783,-3.19915565419569,340.31889052342));
#70160=CARTESIAN_POINT('Ctrl Pts',(58.7407210927044,2.74152182269945,340.568595100703));
#70161=CARTESIAN_POINT('Ctrl Pts',(58.4624830584305,6.16634518769909,335.708082146398));
#70162=CARTESIAN_POINT('Ctrl Pts',(58.1842450241564,3.93240458905305,330.197772657621));
#70163=CARTESIAN_POINT('Ctrl Pts',(57.9060069898825,-1.91024565877038,329.094396320183));
#70164=CARTESIAN_POINT('Ctrl Pts',(57.6277689556085,-5.99989166071994,333.410505313149));
#70165=CARTESIAN_POINT('Ctrl Pts',(57.3495309213347,-4.58352564388255,339.185270119332));
#70166=CARTESIAN_POINT('Ctrl Pts',(57.0712928870607,1.03907420361824,341.119274311492));
#70167=CARTESIAN_POINT('Ctrl Pts',(56.7930548527868,5.70813099116869,337.437710788336));
#70168=CARTESIAN_POINT('Ctrl Pts',(56.5148168185127,5.13892021999894,331.519096055276));
#70169=CARTESIAN_POINT('Ctrl Pts',(56.2365787842391,-0.146201786725707,
328.794855494232));
#70170=CARTESIAN_POINT('Ctrl Pts',(55.9583407499648,-5.29715657170701,331.764984458348));
#70171=CARTESIAN_POINT('Ctrl Pts',(55.6801027156911,-5.58698895673563,337.703839436287));
#70172=CARTESIAN_POINT('Ctrl Pts',(55.401864681417,-0.74972403998978,341.16142087215));
#70173=CARTESIAN_POINT('Ctrl Pts',(55.1236266471431,4.775551562346,338.964757316064));
#70174=CARTESIAN_POINT('Ctrl Pts',(54.8453886128692,5.91837398294238,333.129694490748));
#70175=CARTESIAN_POINT('Ctrl Pts',(54.5671505785953,1.62999195444933,329.010983425608));
#70176=CARTESIAN_POINT('Ctrl Pts',(54.2889125443213,-4.15420963200005,330.388304473048));
#70177=CARTESIAN_POINT('Ctrl Pts',(54.0106745100473,-6.12615435519665,335.997710437058));
#70178=CARTESIAN_POINT('Ctrl Pts',(53.7324364757735,-2.47621764851933,340.691532259161));
#70179=CARTESIAN_POINT('Ctrl Pts',(53.4541984414994,3.44610744529158,340.16231893391));
#70180=CARTESIAN_POINT('Ctrl Pts',(53.1759604072256,6.20599060102094,334.895721718714));
#70181=CARTESIAN_POINT('Ctrl Pts',(52.8977223729516,3.2707277824645,329.724819143107));
#70182=CARTESIAN_POINT('Ctrl Pts',(52.6194843386776,-2.66603364619667,329.394872178331));
#70183=CARTESIAN_POINT('Ctrl Pts',(52.3412463044037,-6.15621534833528,334.208668283948));
#70184=CARTESIAN_POINT('Ctrl Pts',(52.0630082701298,-3.99692909089618,339.74865782535));
#70185=CARTESIAN_POINT('Ctrl Pts',(51.7847702358559,1.83027999868166,340.930874170501));
#70186=CARTESIAN_POINT('Ctrl Pts',(51.506532201582,5.97786814835784,336.670414828945));
#70187=CARTESIAN_POINT('Ctrl Pts',(51.2282941673079,4.63965493147527,330.877040454146));
#70188=CARTESIAN_POINT('Ctrl Pts',(50.9500561330343,-0.95630113482762,328.867245199796));
#70189=CARTESIAN_POINT('Ctrl Pts',(50.67181809876,-5.67467376468082,332.485388506279));
#70190=CARTESIAN_POINT('Ctrl Pts',(50.3935800644862,-5.1854820387339,338.411153664947));
#70191=CARTESIAN_POINT('Ctrl Pts',(50.1153420302121,0.0623500165696838,
341.206553453837));
#70192=CARTESIAN_POINT('Ctrl Pts',(49.8371039959383,5.25296438195201,338.306290746721));
#70193=CARTESIAN_POINT('Ctrl Pts',(49.5588659616644,5.62301086764414,332.371893822109));
#70194=CARTESIAN_POINT('Ctrl Pts',(49.2806279273904,0.832903275603628,328.849271146165));
#70195=CARTESIAN_POINT('Ctrl Pts',(49.0023898931164,-4.72154735882616,330.971081554776));
#70196=CARTESIAN_POINT('Ctrl Pts',(48.7241518588426,-5.94310367198592,336.790170953829));
#70197=CARTESIAN_POINT('Ctrl Pts',(48.4459138245685,-1.71076146543087,340.966446891435));
#70198=CARTESIAN_POINT('Ctrl Pts',(48.1676757902947,4.09152128715226,339.667402581381));
#70199=CARTESIAN_POINT('Ctrl Pts',(47.8894377560206,6.13907534527108,334.085151813145));
#70200=CARTESIAN_POINT('Ctrl Pts',(47.611199721747,2.5528905716382,329.342443722848));
#70201=CARTESIAN_POINT('Ctrl Pts',(47.3329616874728,-3.37604419898399,329.7915915227));
#70202=CARTESIAN_POINT('Ctrl Pts',(47.0547236531989,-6.20683303852926,335.020418906187));
#70203=CARTESIAN_POINT('Ctrl Pts',(46.7764856189251,-3.34170281132171,340.230508160849));
#70204=CARTESIAN_POINT('Ctrl Pts',(46.498247584651,2.59005876238313,340.640637278474));
#70205=CARTESIAN_POINT('Ctrl Pts',(46.2200095503771,6.14496163905365,335.874436821312));
#70206=CARTESIAN_POINT('Ctrl Pts',(45.9417715161031,4.06072391904974,330.305778599899));
#70207=CARTESIAN_POINT('Ctrl Pts',(45.6635334818292,-1.7499802052793,329.044938070764));
#70208=CARTESIAN_POINT('Ctrl Pts',(45.3852954475554,-5.95475332488903,333.248969977519));
#70209=CARTESIAN_POINT('Ctrl Pts',(45.1070574132813,-4.69493721026309,339.059896290744));
#70210=CARTESIAN_POINT('Ctrl Pts',(44.8288193790074,0.873353485061651,341.145115701924));
#70211=CARTESIAN_POINT('Ctrl Pts',(44.5505813447335,5.64018057782164,337.591053135208));
#70212=CARTESIAN_POINT('Ctrl Pts',(44.2723433104595,5.23109720324356,331.659219350193));
#70213=CARTESIAN_POINT('Ctrl Pts',(43.9941052761856,0.0215131361170371,
328.793170657663));
#70214=CARTESIAN_POINT('Ctrl Pts',(43.7158672419116,-5.20781321849073,331.623037639946));
#70215=CARTESIAN_POINT('Ctrl Pts',(43.4376292076377,-5.65800624968665,337.551893136167));
#70216=CARTESIAN_POINT('Ctrl Pts',(43.1593911733638,-0.915930457580677,
341.138913967208));
#70217=CARTESIAN_POINT('Ctrl Pts',(42.8811531390898,4.66668119633548,339.092344060764));
#70218=CARTESIAN_POINT('Ctrl Pts',(42.602915104816,5.96674839647658,333.290290412657));
#70219=CARTESIAN_POINT('Ctrl Pts',(42.3246770705419,1.79121866223313,329.057212017582));
#70220=CARTESIAN_POINT('Ctrl Pts',(42.0464390362682,-4.02808599999753,330.277742438566));
#70221=CARTESIAN_POINT('Ctrl Pts',(41.768201001994,-6.15087559448237,335.831818923268));
#70222=CARTESIAN_POINT('Ctrl Pts',(41.4899629677202,-2.62909744268569,340.622547459718));
#70223=CARTESIAN_POINT('Ctrl Pts',(41.2117249334461,3.305364626849,340.253547181046));
#70224=CARTESIAN_POINT('Ctrl Pts',(40.9334868991725,6.20654236542629,335.06344419656));
#70225=CARTESIAN_POINT('Ctrl Pts',(40.6552488648983,3.41206778366701,329.815119409323));
#70226=CARTESIAN_POINT('Ctrl Pts',(40.3770108306245,-2.51361104112554,329.324883011441));
#70227=CARTESIAN_POINT('Ctrl Pts',(40.0987727963505,-6.13258611431534,334.042617709367));
#70228=CARTESIAN_POINT('Ctrl Pts',(39.8205347620765,-4.12377742722061,339.638928004471));
#70229=CARTESIAN_POINT('Ctrl Pts',(39.5422967278027,1.6693609379794,340.978162540334));
#70230=CARTESIAN_POINT('Ctrl Pts',(39.2640586935287,5.9305514101228,336.83132555047));
#70231=CARTESIAN_POINT('Ctrl Pts',(38.9858206592547,4.74936238799182,331.003908133258));
#70232=CARTESIAN_POINT('Ctrl Pts',(38.7075826249808,-0.79024639712531,328.843645239938));
#70233=CARTESIAN_POINT('Ctrl Pts',(38.4293445907068,-5.60465772761824,332.332978242278));
#70234=CARTESIAN_POINT('Ctrl Pts',(38.1511065564329,-5.27575738608837,338.269797746504));
#70235=CARTESIAN_POINT('Ctrl Pts',(37.872868522159,-0.105372361396576,341.205972120898));
#70236=CARTESIAN_POINT('Ctrl Pts',(37.594630487885,5.16171132405535,338.447017479942));
#70237=CARTESIAN_POINT('Ctrl Pts',(37.3163924536112,5.69196871415593,332.524785775537));
#70238=CARTESIAN_POINT('Ctrl Pts',(37.0381544193371,0.99879042859613,328.874021630821));
#70239=CARTESIAN_POINT('Ctrl Pts',(36.7599163850632,-4.61096309116378,330.844977416206));
#70240=CARTESIAN_POINT('Ctrl Pts',(36.4816783507893,-5.98930383986636,336.628936098708));
#70241=CARTESIAN_POINT('Ctrl Pts',(36.2034403165153,-1.87134885670335,340.918044166481));
#70242=CARTESIAN_POINT('Ctrl Pts',(35.9252022822415,3.96391535119249,339.776250452865));
#70243=CARTESIAN_POINT('Ctrl Pts',(35.6469642479676,6.16155294859364,334.251362195994));
#70244=CARTESIAN_POINT('Ctrl Pts',(35.3687262136935,2.70482434944287,329.413487801986));
#70245=CARTESIAN_POINT('Ctrl Pts',(35.0904881794196,-3.23408163204968,329.702273195308));
#70246=CARTESIAN_POINT('Ctrl Pts',(34.8122501451456,-6.20511863477687,334.852704282978));
#70247=CARTESIAN_POINT('Ctrl Pts',(34.5340121108717,-3.48180985377025,340.138306476077));
#70248=CARTESIAN_POINT('Ctrl Pts',(34.2557740765978,2.43670443861214,340.70856065736));
#70249=CARTESIAN_POINT('Ctrl Pts',(33.9775360423238,6.11909103337872,336.0401529816));
#70250=CARTESIAN_POINT('Ctrl Pts',(33.69929800805,4.18607810444926,330.41721226726));
#70251=CARTESIAN_POINT('Ctrl Pts',(33.421059973776,-1.58843691452174,328.999828213418));
#70252=CARTESIAN_POINT('Ctrl Pts',(33.1428219395021,-5.90526682232657,333.088713245733));
#70253=CARTESIAN_POINT('Ctrl Pts',(32.864583905228,-4.80292052887772,338.931557921892));
#70254=CARTESIAN_POINT('Ctrl Pts',(32.5863458709542,0.706995042931406,341.166469922831));
#70255=CARTESIAN_POINT('Ctrl Pts',(32.3081078366801,5.56811169907211,337.742503492534));
#70256=CARTESIAN_POINT('Ctrl Pts',(32.0298698024063,5.31945443416831,331.801782086425));
#70257=CARTESIAN_POINT('Ctrl Pts',(31.7516317681322,0.189212350046987,328.796018053983));
#70258=CARTESIAN_POINT('Ctrl Pts',(31.4733937338585,-5.11466711494274,331.483556682778));
#70259=CARTESIAN_POINT('Ctrl Pts',(31.1951556995843,-5.72489206091239,337.39808344117));
#70260=CARTESIAN_POINT('Ctrl Pts',(30.9169176653106,-1.08146806185105,341.111924421253));
#70261=CARTESIAN_POINT('Ctrl Pts',(30.6386796310364,4.55440321512858,339.216942571809));
#70262=CARTESIAN_POINT('Ctrl Pts',(30.3604415967627,6.01076588446597,333.452134766186));
#70263=CARTESIAN_POINT('Ctrl Pts',(30.0822035624886,1.95113742038797,329.107780039181));
#70264=CARTESIAN_POINT('Ctrl Pts',(29.8039655282148,-3.89902105563896,330.170628601195));
#70265=CARTESIAN_POINT('Ctrl Pts',(29.5257274939408,-6.17110545836244,335.665320014488));
#70266=CARTESIAN_POINT('Ctrl Pts',(29.2474894596669,-2.78005746731399,340.549457070591));
#70267=CARTESIAN_POINT('Ctrl Pts',(28.9692514253929,3.16220822790757,340.340939282866));
#70268=CARTESIAN_POINT('Ctrl Pts',(28.691013391119,6.20256210649528,335.231120347389));
#70269=CARTESIAN_POINT('Ctrl Pts',(28.412775356845,3.5509162896189,329.909205680443));
#70270=CARTESIAN_POINT('Ctrl Pts',(28.1345373225713,-2.35935299480223,329.259037820555));
#70271=CARTESIAN_POINT('Ctrl Pts',(27.8562992882971,-6.10447885988647,333.877266216279));
#70272=CARTESIAN_POINT('Ctrl Pts',(27.5780612540233,-4.24761457721317,339.525810833801));
#70273=CARTESIAN_POINT('Ctrl Pts',(27.2998232197493,1.50722290828026,341.021085650003));
#70274=CARTESIAN_POINT('Ctrl Pts',(27.0215851854754,5.87890417741855,336.990899036275));
#70275=CARTESIAN_POINT('Ctrl Pts',(26.7433471512014,4.85560185542327,331.133693762579));
#70276=CARTESIAN_POINT('Ctrl Pts',(26.4651091169276,-0.62361462072805,328.824540656379));
#70277=CARTESIAN_POINT('Ctrl Pts',(26.1868710826535,-5.53054916397395,332.182515440188));
#70278=CARTESIAN_POINT('Ctrl Pts',(25.9086330483796,-5.36218037021281,338.126054218534));
#70279=CARTESIAN_POINT('Ctrl Pts',(25.6303950141058,-0.273017796359905,
341.200859181014));
#70280=CARTESIAN_POINT('Ctrl Pts',(25.3521569798317,5.06668917947642,338.585227197611));
#70281=CARTESIAN_POINT('Ctrl Pts',(25.0739189455577,5.75677027951692,332.679485132825));
#70282=CARTESIAN_POINT('Ctrl Pts',(24.7956809112839,1.1639482638348,328.903245310903));
#70283=CARTESIAN_POINT('Ctrl Pts',(24.5174428770099,-4.49701189372031,330.721907279214));
#70284=CARTESIAN_POINT('Ctrl Pts',(24.239204842736,-6.03113061219504,336.466511792845));
#70285=CARTESIAN_POINT('Ctrl Pts',(23.960966808462,-2.0305697872003,340.865320079861));
#70286=CARTESIAN_POINT('Ctrl Pts',(23.6827287741881,3.83341496034723,339.881610701572));
#70287=CARTESIAN_POINT('Ctrl Pts',(23.4044907399142,6.17953137989617,334.418119234905));
#70288=CARTESIAN_POINT('Ctrl Pts',(23.1262527056403,2.85478306184805,329.488611157822));
#70289=CARTESIAN_POINT('Ctrl Pts',(22.8480146713663,-3.0897575355291,329.616823273238));
#70290=CARTESIAN_POINT('Ctrl Pts',(22.5697766370923,-6.19887324729767,334.685097215247));
#70291=CARTESIAN_POINT('Ctrl Pts',(22.2915386028184,-3.61937447524032,340.042352794865));
#70292=CARTESIAN_POINT('Ctrl Pts',(22.0133005685444,2.28157083086538,340.772315639642));
#70293=CARTESIAN_POINT('Ctrl Pts',(21.7350625342706,6.08875226141619,336.205109621158));
#70294=CARTESIAN_POINT('Ctrl Pts',(21.4568244999966,4.30837561150147,330.531992290727));
#70295=CARTESIAN_POINT('Ctrl Pts',(21.1785864657227,-1.4257337455679,328.95909968741));
#70296=CARTESIAN_POINT('Ctrl Pts',(20.9003484314487,-5.85146828812547,332.929852137414));
#70297=CARTESIAN_POINT('Ctrl Pts',(20.6221103971749,-4.90739675020082,338.800348725582));
#70298=CARTESIAN_POINT('Ctrl Pts',(20.3438723629008,0.540120352325815,341.183321381337));
#70299=CARTESIAN_POINT('Ctrl Pts',(20.0656343286271,5.49197697968639,337.891951271115));
#70300=CARTESIAN_POINT('Ctrl Pts',(19.787396294353,5.40392739423611,331.94668016452));
#70301=CARTESIAN_POINT('Ctrl Pts',(19.5091582600792,0.356773400932937,328.803395604019));
#70302=CARTESIAN_POINT('Ctrl Pts',(19.2309202258051,-5.01778627643961,331.346643435978));
#70303=CARTESIAN_POINT('Ctrl Pts',(18.9526821915312,-5.78759755032758,337.242522663286));
#70304=CARTESIAN_POINT('Ctrl Pts',(18.6744441572573,-1.24621597707973,341.080471942077));
#70305=CARTESIAN_POINT('Ctrl Pts',(18.3962061229834,4.43879960421651,339.338461867242));
#70306=CARTESIAN_POINT('Ctrl Pts',(18.1179680887094,6.05039430529802,333.615109372432));
#70307=CARTESIAN_POINT('Ctrl Pts',(17.8397300544354,2.1096314560811,329.162650565589));
#70308=CARTESIAN_POINT('Ctrl Pts',(17.5614920201615,-3.76710904227219,330.067041175568));
#70309=CARTESIAN_POINT('Ctrl Pts',(17.2832539858876,-6.18682917497063,335.498335288377));
#70310=CARTESIAN_POINT('Ctrl Pts',(17.0050159516137,-2.92898749124742,340.472314462457));
#70311=CARTESIAN_POINT('Ctrl Pts',(16.7267779173396,3.01674278140895,340.424431425571));
#70312=CARTESIAN_POINT('Ctrl Pts',(16.4485398830658,6.19405273061698,335.398627733914));
#70313=CARTESIAN_POINT('Ctrl Pts',(16.1703018487919,3.68717191300587,330.00700925458));
#70314=CARTESIAN_POINT('Ctrl Pts',(15.8920638145178,-2.20337214660178,329.197384685895));
#70315=CARTESIAN_POINT('Ctrl Pts',(15.6138257802439,-6.07191410899394,333.712734544503));
#70316=CARTESIAN_POINT('Ctrl Pts',(15.3355877459701,-4.36835011486507,339.409388911613));
#70317=CARTESIAN_POINT('Ctrl Pts',(15.057349711696,1.3439843029285,341.059612157009));
#70318=CARTESIAN_POINT('Ctrl Pts',(14.7791116774222,5.82296416310975,337.149018765648));
#70319=CARTESIAN_POINT('Ctrl Pts',(14.5008736431483,4.95829575759767,331.266302572513));
#70320=CARTESIAN_POINT('Ctrl Pts',(14.2226356088742,-0.456527480302993,
328.809945399307));
#70321=CARTESIAN_POINT('Ctrl Pts',(13.9443975746004,-5.4524021879272,332.034109968084));
#70322=CARTESIAN_POINT('Ctrl Pts',(13.6661595403263,-5.44468788489596,337.980028042719));
#70323=CARTESIAN_POINT('Ctrl Pts',(13.3879215060525,-0.440463873581898,
341.191218367626));
#70324=CARTESIAN_POINT('Ctrl Pts',(13.1096834717786,4.96796733370652,338.720818978924));
#70325=CARTESIAN_POINT('Ctrl Pts',(12.8314454375045,5.81736824512882,332.835878932219));
#70326=CARTESIAN_POINT('Ctrl Pts',(12.5532074032307,1.32825618372396,328.936920847501));
#70327=CARTESIAN_POINT('Ctrl Pts',(12.2749693689567,-4.37977697531212,330.601961009263));
#70328=CARTESIAN_POINT('Ctrl Pts',(11.9967313346828,-6.0685534441121,336.303016639511));
#70329=CARTESIAN_POINT('Ctrl Pts',(11.7184933004087,-2.18830799913804,340.808313129084));
#70330=CARTESIAN_POINT('Ctrl Pts',(11.4402552661348,3.70011541650439,339.983406396494));
#70331=CARTESIAN_POINT('Ctrl Pts',(11.162017231861,6.19299749171987,334.585301157778));
#70332=CARTESIAN_POINT('Ctrl Pts',(10.883779197587,3.00265724584708,329.567758946434));
#70333=CARTESIAN_POINT('Ctrl Pts',(10.6055411633131,-2.94317736486522,329.535304130909));
#70334=CARTESIAN_POINT('Ctrl Pts',(10.327303129039,-6.18810130459427,334.517720129862));
#70335=CARTESIAN_POINT('Ctrl Pts',(10.0490650947653,-3.75429647493768,339.942717107111));
#70336=CARTESIAN_POINT('Ctrl Pts',(9.77082706049122,2.12477168806704,340.831855814069));
#70337=CARTESIAN_POINT('Ctrl Pts',(9.49258902621731,6.05396658870994,336.36918601904));
#70338=CARTESIAN_POINT('Ctrl Pts',(9.21435099194333,4.42752881490187,330.650035366585));
#70339=CARTESIAN_POINT('Ctrl Pts',(8.93611295766945,-1.26199266991894,328.922781272086));
#70340=CARTESIAN_POINT('Ctrl Pts',(8.65787492339546,-5.79339102894519,332.772504467024));
#70341=CARTESIAN_POINT('Ctrl Pts',(8.37963688912154,-5.00830087154158,338.666361085838));
#70342=CARTESIAN_POINT('Ctrl Pts',(8.1013988548476,0.372872575477468,341.1956642397));
#70343=CARTESIAN_POINT('Ctrl Pts',(7.82316082057367,5.4117917753666,338.039275132633));
#70344=CARTESIAN_POINT('Ctrl Pts',(7.54492278629972,5.48453037873516,332.093830837367));
#70345=CARTESIAN_POINT('Ctrl Pts',(7.26668475202578,0.52393047366258,328.815254383241));
#70346=CARTESIAN_POINT('Ctrl Pts',(6.98844671775185,-4.91697055337583,331.212480081138));
#70347=CARTESIAN_POINT('Ctrl Pts',(6.71020868347791,-5.84658848615386,337.085169169869));
#70348=CARTESIAN_POINT('Ctrl Pts',(6.43197064920395,-1.40908752098961,341.044872581102));
#70349=CARTESIAN_POINT('Ctrl Pts',(6.15373261493005,4.31812627429368,339.456259878022));
#70350=CARTESIAN_POINT('Ctrl Pts',(5.87549458065607,6.08908817465391,333.780139476516));
#70351=CARTESIAN_POINT('Ctrl Pts',(5.59725654638217,2.25975513930278,329.219816699493));
#70352=CARTESIAN_POINT('Ctrl Pts',(5.36539151782054,-2.6379404393598,329.845549066121));
#70353=CARTESIAN_POINT('Ctrl Pts',(5.17989949497124,-4.93068027107053,332.649384088804));
#70354=CARTESIAN_POINT('Ctrl Pts',(5.08715348354661,-5.28802671673104,334.407219181606));
#70355=CARTESIAN_POINT('Ctrl Pts',(5.04078047783429,-5.24142383043492,335.279901837379));
#70356=CARTESIAN_POINT('Ctrl Pts',(185.423459434742,-2.43876419493702,329.976059081413));
#70357=CARTESIAN_POINT('Ctrl Pts',(185.377084700732,-3.27526837515656,330.38212144629));
#70358=CARTESIAN_POINT('Ctrl Pts',(185.284336961008,-4.72780408125933,331.620144579983));
#70359=CARTESIAN_POINT('Ctrl Pts',(185.098843209861,-6.15736430490123,335.198742348302));
#70360=CARTESIAN_POINT('Ctrl Pts',(184.866978181299,-4.21750050188893,340.080738627298));
#70361=CARTESIAN_POINT('Ctrl Pts',(184.588740147026,2.00032595301521,341.297165656258));
#70362=CARTESIAN_POINT('Ctrl Pts',(184.31050211275,6.37268333620086,336.725085768952));
#70363=CARTESIAN_POINT('Ctrl Pts',(184.032264078478,4.90203688689787,330.574908170056));
#70364=CARTESIAN_POINT('Ctrl Pts',(183.754026044204,-1.06983530224133,328.482947982007));
#70365=CARTESIAN_POINT('Ctrl Pts',(183.47578800993,-6.0585072503333,332.372977788209));
#70366=CARTESIAN_POINT('Ctrl Pts',(183.197549975656,-5.4881327455372,338.673052515815));
#70367=CARTESIAN_POINT('Ctrl Pts',(182.919311941382,0.119020659026097,341.60281017205));
#70368=CARTESIAN_POINT('Ctrl Pts',(182.641073907107,5.61673846577441,338.473060374359));
#70369=CARTESIAN_POINT('Ctrl Pts',(182.362835872834,5.9601706119106,332.156243440002));
#70370=CARTESIAN_POINT('Ctrl Pts',(182.084597838559,0.833982670938808,328.449042143749));
#70371=CARTESIAN_POINT('Ctrl Pts',(181.806359804286,-5.05750735223084,330.753588782418));
#70372=CARTESIAN_POINT('Ctrl Pts',(181.528121770012,-6.30781421230692,336.954988111478));
#70373=CARTESIAN_POINT('Ctrl Pts',(181.249883735738,-1.76952423629996,341.362332289535));
#70374=CARTESIAN_POINT('Ctrl Pts',(180.971645701464,4.39262733330804,339.931053487594));
#70375=CARTESIAN_POINT('Ctrl Pts',(180.69340766719,6.52373211271479,333.974622089771));
#70376=CARTESIAN_POINT('Ctrl Pts',(180.415169632916,2.66810290978665,328.959163590617));
#70377=CARTESIAN_POINT('Ctrl Pts',(180.136931598643,-3.63600425714706,329.487292176997));
#70378=CARTESIAN_POINT('Ctrl Pts',(179.858693564369,-6.60340435279722,335.074351007501));
#70379=CARTESIAN_POINT('Ctrl Pts',(179.580455530094,-3.51095754499201,340.593179205234));
#70380=CARTESIAN_POINT('Ctrl Pts',(179.302217495821,2.80344307694077,340.97922930121));
#70381=CARTESIAN_POINT('Ctrl Pts',(179.023979461547,6.54516542060559,335.878228973867));
#70382=CARTESIAN_POINT('Ctrl Pts',(178.745741427273,4.28048603530062,329.971290851712));
#70383=CARTESIAN_POINT('Ctrl Pts',(178.467503392998,-1.91233218939032,328.679124906215));
#70384=CARTESIAN_POINT('Ctrl Pts',(178.189265358724,-6.35023139797826,333.187532730431));
#70385=CARTESIAN_POINT('Ctrl Pts',(177.911027324451,-4.96061697760105,339.359215020136));
#70386=CARTESIAN_POINT('Ctrl Pts',(177.632789290177,0.981282422255545,341.530510025558));
#70387=CARTESIAN_POINT('Ctrl Pts',(177.354551255903,6.02267342811975,337.708852371867));
#70388=CARTESIAN_POINT('Ctrl Pts',(177.07631322163,5.53714592287347,331.401320878489));
#70389=CARTESIAN_POINT('Ctrl Pts',(176.798075187355,-0.029738667315452,
328.396244098834));
#70390=CARTESIAN_POINT('Ctrl Pts',(176.51983715308,-5.56933252163025,331.451336638226));
#70391=CARTESIAN_POINT('Ctrl Pts',(176.241599118807,-5.99803212396333,337.762985166628));
#70392=CARTESIAN_POINT('Ctrl Pts',(175.963361084532,-0.922426176994555,
341.539082989158));
#70393=CARTESIAN_POINT('Ctrl Pts',(175.685123050259,4.99967665764068,339.314360869272));
#70394=CARTESIAN_POINT('Ctrl Pts',(175.406885015986,6.33365001865148,333.130413459503));
#70395=CARTESIAN_POINT('Ctrl Pts',(175.128646981712,1.85532624207433,328.662158022904));
#70396=CARTESIAN_POINT('Ctrl Pts',(174.850408947438,-4.32560304228792,330.010046622287));
#70397=CARTESIAN_POINT('Ctrl Pts',(174.572170913164,-6.53699026053673,335.937141784809));
#70398=CARTESIAN_POINT('Ctrl Pts',(174.29393287889,-2.74947800251017,341.004235763601));
#70399=CARTESIAN_POINT('Ctrl Pts',(174.015694844616,3.56118963619175,340.561331204512));
#70400=CARTESIAN_POINT('Ctrl Pts',(173.737456810342,6.60380610883307,335.014875084156));
#70401=CARTESIAN_POINT('Ctrl Pts',(173.459218776068,3.58620718741687,329.454768318626));
#70402=CARTESIAN_POINT('Ctrl Pts',(173.180980741794,-2.72240113756057,328.983438819608));
#70403=CARTESIAN_POINT('Ctrl Pts',(172.90274270752,-6.53270212117353,334.033418711538));
#70404=CARTESIAN_POINT('Ctrl Pts',(172.624504673246,-4.34803879071085,339.970415985173));
#70405=CARTESIAN_POINT('Ctrl Pts',(172.346266638971,1.82675556103984,341.346135872435));
#70406=CARTESIAN_POINT('Ctrl Pts',(172.068028604698,6.32516329729214,336.898100538374));
#70407=CARTESIAN_POINT('Ctrl Pts',(171.789790570425,5.0190620348767,330.708206356167));
#70408=CARTESIAN_POINT('Ctrl Pts',(171.51155253615,-0.892958375710887,328.456827854133));
#70409=CARTESIAN_POINT('Ctrl Pts',(171.233314501877,-5.98552406495261,332.2100218533));
#70410=CARTESIAN_POINT('Ctrl Pts',(170.955076467602,-5.58526266597773,338.523537617683));
#70411=CARTESIAN_POINT('Ctrl Pts',(170.676838433328,-0.0594881567769249,
341.603554917649));
#70412=CARTESIAN_POINT('Ctrl Pts',(170.398600399054,5.52087775585432,338.623587337999));
#70413=CARTESIAN_POINT('Ctrl Pts',(170.120362364781,6.03481563996016,332.318307142329));
#70414=CARTESIAN_POINT('Ctrl Pts',(169.842124330507,1.01069228500742,328.473976900422));
#70415=CARTESIAN_POINT('Ctrl Pts',(169.563886296233,-4.94092846210296,330.618481733055));
#70416=CARTESIAN_POINT('Ctrl Pts',(169.285648261959,-6.35833208752602,336.783841208159));
#70417=CARTESIAN_POINT('Ctrl Pts',(169.007410227685,-1.94078820505423,341.312195935989));
#70418=CARTESIAN_POINT('Ctrl Pts',(168.729172193411,4.25778836720887,340.04794162122));
#70419=CARTESIAN_POINT('Ctrl Pts',(168.450934159137,6.54905539973767,334.151265788155));
#70420=CARTESIAN_POINT('Ctrl Pts',(168.172696124863,2.83035095582653,329.033460814003));
#70421=CARTESIAN_POINT('Ctrl Pts',(167.894458090589,-3.48572478433498,329.391060784866));
#70422=CARTESIAN_POINT('Ctrl Pts',(167.616220056316,-6.60300233912578,334.895901485651));
#70423=CARTESIAN_POINT('Ctrl Pts',(167.337982022041,-3.66080210745563,340.496271856563));
#70424=CARTESIAN_POINT('Ctrl Pts',(167.059743987767,2.64086218487603,341.052794669545));
#70425=CARTESIAN_POINT('Ctrl Pts',(166.781505953493,6.51904622920892,336.054757153391));
#70426=CARTESIAN_POINT('Ctrl Pts',(166.503267919219,4.41479776996139,330.088784565758));
#70427=CARTESIAN_POINT('Ctrl Pts',(166.225029884946,-1.74084544047143,328.62976189271));
#70428=CARTESIAN_POINT('Ctrl Pts',(165.946791850672,-6.2989404850202,333.01661270616));
#70429=CARTESIAN_POINT('Ctrl Pts',(165.668553816398,-5.07659081867508,339.22358876442));
#70430=CARTESIAN_POINT('Ctrl Pts',(165.390315782124,0.804471311610485,341.55463975364));
#70431=CARTESIAN_POINT('Ctrl Pts',(165.11207774785,5.94728199320819,337.870594587267));
#70432=CARTESIAN_POINT('Ctrl Pts',(164.833839713576,5.63235977137711,331.552247138068));
#70433=CARTESIAN_POINT('Ctrl Pts',(164.555601679302,0.148704120847259,328.397851601514));
#70434=CARTESIAN_POINT('Ctrl Pts',(164.277363645027,-5.47141510651493,331.3021502027));
#70435=CARTESIAN_POINT('Ctrl Pts',(163.999125610754,-6.07049744858296,337.599910982695));
#70436=CARTESIAN_POINT('Ctrl Pts',(163.72088757648,-1.09877388248187,341.511771828493));
#70437=CARTESIAN_POINT('Ctrl Pts',(163.442649542206,4.8812782576969,339.447875780879));
#70438=CARTESIAN_POINT('Ctrl Pts',(163.164411507932,6.38185338833623,333.30222977969));
#70439=CARTESIAN_POINT('Ctrl Pts',(162.886173473658,2.02589586050099,328.714602450632));
#70440=CARTESIAN_POINT('Ctrl Pts',(162.607935439384,-4.18919639634211,329.894991680314));
#70441=CARTESIAN_POINT('Ctrl Pts',(162.329697405111,-6.5599249526995,335.760171695172));
#70442=CARTESIAN_POINT('Ctrl Pts',(162.051459370836,-2.91070720429822,340.927753365486));
#70443=CARTESIAN_POINT('Ctrl Pts',(161.773221336563,3.40962358351962,340.655523265791));
#70444=CARTESIAN_POINT('Ctrl Pts',(161.494983302289,6.60099313470312,335.193302940465));
#70445=CARTESIAN_POINT('Ctrl Pts',(161.216745268015,3.73472871666854,329.553691359822));
#70446=CARTESIAN_POINT('Ctrl Pts',(160.938507233741,-2.55884112014728,328.912076830886));
#70447=CARTESIAN_POINT('Ctrl Pts',(160.660269199467,-6.50420022943695,333.857259536647));
#70448=CARTESIAN_POINT('Ctrl Pts',(160.382031165193,-4.48075079001036,339.851118298805));
#70449=CARTESIAN_POINT('Ctrl Pts',(160.103793130919,1.65461751363549,341.393177400539));
#70450=CARTESIAN_POINT('Ctrl Pts',(159.825555096645,6.27156774713252,337.068311964941));
#70451=CARTESIAN_POINT('Ctrl Pts',(159.547317062371,5.13319282727425,330.845387167351));
#70452=CARTESIAN_POINT('Ctrl Pts',(159.269079028097,-0.715837384371603,
328.435089244298));
#70453=CARTESIAN_POINT('Ctrl Pts',(158.990840993823,-5.90795419412213,332.049313023829));
#70454=CARTESIAN_POINT('Ctrl Pts',(158.712602959549,-5.67842864118778,338.371338689323));
#70455=CARTESIAN_POINT('Ctrl Pts',(158.434364925275,-0.237892937704753,
341.599536600503));
#70456=CARTESIAN_POINT('Ctrl Pts',(158.156126891001,5.42095360341592,338.771437182402));
#70457=CARTESIAN_POINT('Ctrl Pts',(157.877888856727,6.10507103582582,332.482345528331));
#70458=CARTESIAN_POINT('Ctrl Pts',(157.599650822454,1.18665488935917,328.503668222393));
#70459=CARTESIAN_POINT('Ctrl Pts',(157.321412788179,-4.82073693407496,330.486578703064));
#70460=CARTESIAN_POINT('Ctrl Pts',(157.043174753906,-6.40420962706899,336.611389289944));
#70461=CARTESIAN_POINT('Ctrl Pts',(156.764936719632,-2.11063367128099,341.257451709509));
#70462=CARTESIAN_POINT('Ctrl Pts',(156.486698685358,4.11983965173963,340.161143055094));
#70463=CARTESIAN_POINT('Ctrl Pts',(156.208460651084,6.56959693509242,334.328529597365));
#70464=CARTESIAN_POINT('Ctrl Pts',(155.93022261681,2.99053207820273,329.112114617248));
#70465=CARTESIAN_POINT('Ctrl Pts',(155.651984582536,-3.33289992667248,329.298925147836));
#70466=CARTESIAN_POINT('Ctrl Pts',(155.373746548262,-6.59777886236264,334.717527922529));
#70467=CARTESIAN_POINT('Ctrl Pts',(155.095508513988,-3.80797351911897,340.395351153436));
#70468=CARTESIAN_POINT('Ctrl Pts',(154.817270479714,2.47635291702316,341.121940266087));
#70469=CARTESIAN_POINT('Ctrl Pts',(154.53903244544,6.48816683212228,336.230515156241));
#70470=CARTESIAN_POINT('Ctrl Pts',(154.260794411166,4.54588581056825,330.209864449886));
#70471=CARTESIAN_POINT('Ctrl Pts',(153.982556376892,-1.56808752217966,328.585050435586));
#70472=CARTESIAN_POINT('Ctrl Pts',(153.704318342618,-6.24305008075718,332.847140952048));
#70473=CARTESIAN_POINT('Ctrl Pts',(153.426080308345,-5.18885772749205,339.084878440669));
#70474=CARTESIAN_POINT('Ctrl Pts',(153.14784227407,0.62707277487803,341.573983276994));
#70475=CARTESIAN_POINT('Ctrl Pts',(152.869604239797,5.86754784732152,338.030240691857));
#70476=CARTESIAN_POINT('Ctrl Pts',(152.591366205523,5.72346086514233,331.705690950081));
#70477=CARTESIAN_POINT('Ctrl Pts',(152.313128171249,0.327038325165903,328.404279999495));
#70478=CARTESIAN_POINT('Ctrl Pts',(152.034890136975,-5.36950245873749,331.155663940705));
#70479=CARTESIAN_POINT('Ctrl Pts',(151.756652102701,-6.13853008998387,337.434938341222));
#70480=CARTESIAN_POINT('Ctrl Pts',(151.478414068427,-1.27431926220765,341.479705765631));
#70481=CARTESIAN_POINT('Ctrl Pts',(151.200176034153,4.75931554357499,339.578142849221));
#70482=CARTESIAN_POINT('Ctrl Pts',(150.921937999879,6.4253967224012,333.475285813359));
#70483=CARTESIAN_POINT('Ctrl Pts',(150.643699965605,2.19498616778012,328.771636481832));
#70484=CARTESIAN_POINT('Ctrl Pts',(150.365461931331,-4.04973079507009,329.783664420433));
#70485=CARTESIAN_POINT('Ctrl Pts',(150.087223897057,-6.57806958121304,335.582646527415));
#70486=CARTESIAN_POINT('Ctrl Pts',(149.808985862783,-3.06981100482464,340.846942516038));
#70487=CARTESIAN_POINT('Ctrl Pts',(149.53074782851,3.25556782035516,340.745585658421));
#70488=CARTESIAN_POINT('Ctrl Pts',(149.252509794235,6.5933601088973,335.371589646777));
#70489=CARTESIAN_POINT('Ctrl Pts',(148.974271759962,3.88052314334006,329.656591300939));
#70490=CARTESIAN_POINT('Ctrl Pts',(148.696033725687,-2.39341263443264,328.845160249647));
#70491=CARTESIAN_POINT('Ctrl Pts',(148.417795691414,-6.47094896429908,333.681934791966));
#70492=CARTESIAN_POINT('Ctrl Pts',(148.13955765714,-4.61019094067841,339.72827832109));
#70493=CARTESIAN_POINT('Ctrl Pts',(147.861319622866,1.4812712628961,341.435550624221));
#70494=CARTESIAN_POINT('Ctrl Pts',(147.583081588592,6.21339269203886,337.237013108077));
#70495=CARTESIAN_POINT('Ctrl Pts',(147.304843554318,5.24357535722337,330.98560168091));
#70496=CARTESIAN_POINT('Ctrl Pts',(147.026605520044,-0.538193687870606,
328.418144338751));
#70497=CARTESIAN_POINT('Ctrl Pts',(146.74836748577,-5.82607032933153,331.890758788889));
#70498=CARTESIAN_POINT('Ctrl Pts',(146.470129451496,-5.76744822222202,338.216678006139));
#70499=CARTESIAN_POINT('Ctrl Pts',(146.191891417222,-0.416124008975574,
341.590699295245));
#70500=CARTESIAN_POINT('Ctrl Pts',(145.913653382948,5.31707106532745,338.916533119666));
#70501=CARTESIAN_POINT('Ctrl Pts',(145.635415348674,6.17086850281975,332.648222308105));
#70502=CARTESIAN_POINT('Ctrl Pts',(145.3571773144,1.36175099714417,328.538103172212));
#70503=CARTESIAN_POINT('Ctrl Pts',(145.078939280126,-4.69702529919884,330.357971377741));
#70504=CARTESIAN_POINT('Ctrl Pts',(144.800701245853,-6.44541080644686,336.437760733685));
#70505=CARTESIAN_POINT('Ctrl Pts',(144.522463211578,-2.27893795072618,341.198138285642));
#70506=CARTESIAN_POINT('Ctrl Pts',(144.244225177305,3.97888262530681,340.270575817235));
#70507=CARTESIAN_POINT('Ctrl Pts',(143.96598714303,6.58534134430714,334.506283714924));
#70508=CARTESIAN_POINT('Ctrl Pts',(143.687749108757,3.14852951111574,329.195067760186));
#70509=CARTESIAN_POINT('Ctrl Pts',(143.409511074483,-3.17764138220717,329.210952441267));
#70510=CARTESIAN_POINT('Ctrl Pts',(143.131273040209,-6.58773768098847,334.539360620795));
#70511=CARTESIAN_POINT('Ctrl Pts',(142.853035005935,-3.95236434477544,340.290490759593));
#70512=CARTESIAN_POINT('Ctrl Pts',(142.574796971661,2.31003541383591,341.186615615829));
#70513=CARTESIAN_POINT('Ctrl Pts',(142.296558937387,6.45254976923686,336.405374635716));
#70514=CARTESIAN_POINT('Ctrl Pts',(142.018320903113,4.67365444088762,330.334442095702));
#70515=CARTESIAN_POINT('Ctrl Pts',(141.740082868839,-1.39418458483772,328.545023180941));
#70516=CARTESIAN_POINT('Ctrl Pts',(141.461844834565,-6.18260099518822,332.679241217728));
#70517=CARTESIAN_POINT('Ctrl Pts',(141.183606800291,-5.29733572729561,338.943185334664));
#70518=CARTESIAN_POINT('Ctrl Pts',(140.905368766017,0.449216348989023,341.588526471297));
#70519=CARTESIAN_POINT('Ctrl Pts',(140.627130731743,5.78352921222887,338.187674111713));
#70520=CARTESIAN_POINT('Ctrl Pts',(140.34889269747,5.81038268215753,331.861540269802));
#70521=CARTESIAN_POINT('Ctrl Pts',(140.070654663195,0.505133725778029,328.415524598705));
#70522=CARTESIAN_POINT('Ctrl Pts',(139.792416628922,-5.26366899498638,331.011984816678));
#70523=CARTESIAN_POINT('Ctrl Pts',(139.514178594648,-6.20208037067882,337.268187705379));
#70524=CARTESIAN_POINT('Ctrl Pts',(139.235940560374,-1.4489341327555,341.44290821525));
#70525=CARTESIAN_POINT('Ctrl Pts',(138.9577025261,4.63387757256473,339.705066953155));
#70526=CARTESIAN_POINT('Ctrl Pts',(138.679464491826,6.46424822546323,333.649455194825));
#70527=CARTESIAN_POINT('Ctrl Pts',(138.401226457552,2.36247369400165,328.833218470195));
#70528=CARTESIAN_POINT('Ctrl Pts',(138.122988423278,-3.90730807639073,329.676146133921));
#70529=CARTESIAN_POINT('Ctrl Pts',(137.844750389004,-6.59141089685199,335.404695910594));
#70530=CARTESIAN_POINT('Ctrl Pts',(137.56651235473,-3.22667322633757,340.761862223415));
#70531=CARTESIAN_POINT('Ctrl Pts',(137.288274320456,3.09913483836811,340.831452618757));
#70532=CARTESIAN_POINT('Ctrl Pts',(137.010036286182,6.58091260505858,335.549605017963));
#70533=CARTESIAN_POINT('Ctrl Pts',(136.731798251908,4.02348400819764,329.763393004342));
#70534=CARTESIAN_POINT('Ctrl Pts',(136.453560217634,-2.22623647645968,328.782737938444));
#70535=CARTESIAN_POINT('Ctrl Pts',(136.17532218336,-6.43297260586646,333.507572499797));
#70536=CARTESIAN_POINT('Ctrl Pts',(135.897084149086,-4.73626472538963,339.601985749893));
#70537=CARTESIAN_POINT('Ctrl Pts',(135.618846114812,1.30684338642453,341.47322460251));
#70538=CARTESIAN_POINT('Ctrl Pts',(135.340608080539,6.15068061149365,337.404080782043));
#70539=CARTESIAN_POINT('Ctrl Pts',(135.062370046264,5.35012902329207,331.128747512067));
#70540=CARTESIAN_POINT('Ctrl Pts',(134.784132011991,-0.360157001809702,
328.406005510677));
#70541=CARTESIAN_POINT('Ctrl Pts',(134.505893977717,-5.73993226225935,331.734474924936));
#70542=CARTESIAN_POINT('Ctrl Pts',(134.227655943443,-5.8522564068949,338.059668501513));
#70543=CARTESIAN_POINT('Ctrl Pts',(133.949417909169,-0.594051226085983,
341.577049454882));
#70544=CARTESIAN_POINT('Ctrl Pts',(133.671179874895,5.20930599672032,339.058769200599));
#70545=CARTESIAN_POINT('Ctrl Pts',(133.392941840621,6.23215999556685,332.815816358259));
#70546=CARTESIAN_POINT('Ctrl Pts',(133.114703806347,1.53585275301256,328.577256605449));
#70547=CARTESIAN_POINT('Ctrl Pts',(132.836465772073,-4.56988389183189,330.23275366628));
#70548=CARTESIAN_POINT('Ctrl Pts',(132.558227737799,-6.48190554051795,336.263082323126));
#70549=CARTESIAN_POINT('Ctrl Pts',(132.279989703525,-2.44557814743964,341.134298975103));
#70550=CARTESIAN_POINT('Ctrl Pts',(132.001751669251,3.83502021486974,340.376159999734));
#70551=CARTESIAN_POINT('Ctrl Pts',(131.723513634977,6.59627713079875,334.684398344598));
#70552=CARTESIAN_POINT('Ctrl Pts',(131.445275600703,3.3042278846846,329.282259670354));
#70553=CARTESIAN_POINT('Ctrl Pts',(131.16703756643,-3.02006252088097,329.127206902916));
#70554=CARTESIAN_POINT('Ctrl Pts',(130.888799532155,-6.57288612708381,334.361529678387));
#70555=CARTESIAN_POINT('Ctrl Pts',(130.610561497882,-4.09386915010205,340.181767244197));
#70556=CARTESIAN_POINT('Ctrl Pts',(130.332323463607,2.14203112051876,341.246773492765));
#70557=CARTESIAN_POINT('Ctrl Pts',(130.054085429334,6.41222104816702,336.579207909249));
#70558=CARTESIAN_POINT('Ctrl Pts',(129.77584739506,4.79801036413993,330.462426536485));
#70559=CARTESIAN_POINT('Ctrl Pts',(129.497609360786,-1.21926361254148,328.509709356714));
#70560=CARTESIAN_POINT('Ctrl Pts',(129.219371326512,-6.117637368295,332.513036103753));
#70561=CARTESIAN_POINT('Ctrl Pts',(128.941133292238,-5.40194560734373,338.798612910852));
#70562=CARTESIAN_POINT('Ctrl Pts',(128.662895257964,0.271031904880399,341.598258717095));
#70563=CARTESIAN_POINT('Ctrl Pts',(128.38465722369,5.69528743842016,338.342779888799));
#70564=CARTESIAN_POINT('Ctrl Pts',(128.106419189416,5.89306175202652,332.019681295903));
#70565=CARTESIAN_POINT('Ctrl Pts',(127.828181155142,0.68286027724717,328.431577188323));
#70566=CARTESIAN_POINT('Ctrl Pts',(127.549943120868,-5.15399199496077,330.871217745259));
#70567=CARTESIAN_POINT('Ctrl Pts',(127.271705086593,-6.26110188619041,337.099780836643));
#70568=CARTESIAN_POINT('Ctrl Pts',(126.99346705232,-1.62249099017548,341.401406046955));
#70569=CARTESIAN_POINT('Ctrl Pts',(126.715229018046,4.50505593959574,339.828555412574));
#70570=CARTESIAN_POINT('Ctrl Pts',(126.436990983773,6.49837952811661,333.824610745435));
#70571=CARTESIAN_POINT('Ctrl Pts',(126.158752949498,2.52823613960948,328.899303448494));
#70572=CARTESIAN_POINT('Ctrl Pts',(125.880514915225,-3.76203223751303,329.572515330735));
#70573=CARTESIAN_POINT('Ctrl Pts',(125.602276880951,-6.59993915777462,335.226449784418));
#70574=CARTESIAN_POINT('Ctrl Pts',(125.324038846677,-3.38117932788874,340.672574613335));
#70575=CARTESIAN_POINT('Ctrl Pts',(125.045800812403,2.94043886507557,340.913061446657));
#70576=CARTESIAN_POINT('Ctrl Pts',(124.767562778129,6.56365971236653,335.727219067027));
#70577=CARTESIAN_POINT('Ctrl Pts',(124.489324743855,4.16350692107729,329.874018483321));
#70578=CARTESIAN_POINT('Ctrl Pts',(124.211086709581,-2.05743471842317,328.72485547811));
#70579=CARTESIAN_POINT('Ctrl Pts',(123.932848675307,-6.39029888451334,333.334299979654));
#70580=CARTESIAN_POINT('Ctrl Pts',(123.654610641033,-4.85888008494255,339.472332804179));
#70581=CARTESIAN_POINT('Ctrl Pts',(123.376372606759,1.13146125162753,341.506171825833));
#70582=CARTESIAN_POINT('Ctrl Pts',(123.098134572485,6.08347729791972,337.569392993857));
#70583=CARTESIAN_POINT('Ctrl Pts',(122.819896538211,5.45277601988872,331.274720135599));
#70584=CARTESIAN_POINT('Ctrl Pts',(122.541658503937,-0.181857328751986,
328.39868162386));
#70585=CARTESIAN_POINT('Ctrl Pts',(122.263420469663,-5.64960289100673,331.580575550605));
#70586=CARTESIAN_POINT('Ctrl Pts',(121.985182435389,-5.93279126818671,337.900424823939));
#70587=CARTESIAN_POINT('Ctrl Pts',(121.706944401116,-0.771544666407324,
341.558597046544));
#70588=CARTESIAN_POINT('Ctrl Pts',(121.428706366841,5.09773708775345,339.198041564269));
#70589=CARTESIAN_POINT('Ctrl Pts',(121.150468332568,6.28890075895896,332.985005301457));
#70590=CARTESIAN_POINT('Ctrl Pts',(120.872230298294,1.70883302769088,328.621099932225));
#70591=CARTESIAN_POINT('Ctrl Pts',(120.59399226402,-4.43940555075498,330.111017002779));
#70592=CARTESIAN_POINT('Ctrl Pts',(120.315754229746,-6.51366718079151,336.087481608612));
#70593=CARTESIAN_POINT('Ctrl Pts',(120.037516195472,-2.61043258058566,341.065980393425));
#70594=CARTESIAN_POINT('Ctrl Pts',(119.759278161198,3.68835746890191,340.477818504914));
#70595=CARTESIAN_POINT('Ctrl Pts',(119.481040126924,6.60239630924522,334.862743426914));
#70596=CARTESIAN_POINT('Ctrl Pts',(119.20280209265,3.45751350780396,329.37362668013));
#70597=CARTESIAN_POINT('Ctrl Pts',(118.924564058376,-2.86027840693326,329.047749683857));
#70598=CARTESIAN_POINT('Ctrl Pts',(118.646326024102,-6.55323504526792,334.184164947638));
#70599=CARTESIAN_POINT('Ctrl Pts',(118.368087989828,-4.23238460815091,340.069259997266));
#70600=CARTESIAN_POINT('Ctrl Pts',(118.089849955554,1.97246271397175,341.302369969558));
#70601=CARTESIAN_POINT('Ctrl Pts',(117.81161192128,6.3672101169845,336.751888043614));
#70602=CARTESIAN_POINT('Ctrl Pts',(117.533373887006,4.91886277550783,330.593724317872));
#70603=CARTESIAN_POINT('Ctrl Pts',(117.255135852733,-1.04345233275681,328.479134749095));
#70604=CARTESIAN_POINT('Ctrl Pts',(116.976897818459,-6.04820663658166,332.34864697326));
#70605=CARTESIAN_POINT('Ctrl Pts',(116.698659784185,-5.50261098139925,338.651266736158));
#70606=CARTESIAN_POINT('Ctrl Pts',(116.420421749911,0.0926495530080822,
341.603172907892));
#70607=CARTESIAN_POINT('Ctrl Pts',(116.142183715637,5.60288696012516,338.495444764725));
#70608=CARTESIAN_POINT('Ctrl Pts',(115.863945681363,5.97143770241139,332.179998553651));
#70609=CARTESIAN_POINT('Ctrl Pts',(115.585707647089,0.860088203470714,328.452426046737));
#70610=CARTESIAN_POINT('Ctrl Pts',(115.307469612815,-5.04055154491398,330.7334655147));
#70611=CARTESIAN_POINT('Ctrl Pts',(115.029231578541,-6.31555153894996,336.929840705875));
#70612=CARTESIAN_POINT('Ctrl Pts',(114.750993544267,-1.79486310307947,341.355229565673));
#70613=CARTESIAN_POINT('Ctrl Pts',(114.472755509993,4.37294471035107,339.948518056085));
#70614=CARTESIAN_POINT('Ctrl Pts',(114.194517475719,6.52776570765055,334.000624566437));
#70615=CARTESIAN_POINT('Ctrl Pts',(113.916279441445,2.69215246470304,328.96984316141));
#70616=CARTESIAN_POINT('Ctrl Pts',(113.638041407171,-3.61400935899722,329.47284768219));
#70617=CARTESIAN_POINT('Ctrl Pts',(113.359803372898,-6.60364813663642,335.048038304389));
#70618=CARTESIAN_POINT('Ctrl Pts',(113.081565338623,-3.53321648897111,340.579144883695));
#70619=CARTESIAN_POINT('Ctrl Pts',(112.80332730435,2.7795957804331,340.990352551276));
#70620=CARTESIAN_POINT('Ctrl Pts',(112.525089270076,6.54161402890032,335.904302100012));
#70621=CARTESIAN_POINT('Ctrl Pts',(112.246851235802,4.30048963711052,329.988386959043));
#70622=CARTESIAN_POINT('Ctrl Pts',(111.968613201528,-1.88713061953261,328.671555134473));
#70623=CARTESIAN_POINT('Ctrl Pts',(111.690375167254,-6.34295896063294,333.162243755305));
#70624=CARTESIAN_POINT('Ctrl Pts',(111.41213713298,-4.97794748548122,339.339414156655));
#70625=CARTESIAN_POINT('Ctrl Pts',(111.133899098706,0.955252922712176,341.534368236092));
#70626=CARTESIAN_POINT('Ctrl Pts',(110.855661064432,6.01183182324263,337.732829032383));
#70627=CARTESIAN_POINT('Ctrl Pts',(110.577423030158,5.55144139407559,331.423412962147));
#70628=CARTESIAN_POINT('Ctrl Pts',(110.299184995884,-0.0034248632939677,
328.396178026211));
#70629=CARTESIAN_POINT('Ctrl Pts',(110.02094696161,-5.55514817416955,331.429173043368));
#70630=CARTESIAN_POINT('Ctrl Pts',(109.742708927336,-6.00899399946238,337.739063253307));
#70631=CARTESIAN_POINT('Ctrl Pts',(109.464470893062,-0.948474724054632,
341.535355544193));
#70632=CARTESIAN_POINT('Ctrl Pts',(109.186232858788,4.98244580615406,339.334248513863));
#70633=CARTESIAN_POINT('Ctrl Pts',(108.907994824514,6.34104936083474,333.155665595764));
#70634=CARTESIAN_POINT('Ctrl Pts',(108.62975679024,1.8805655108125,328.669601138101));
#70635=CARTESIAN_POINT('Ctrl Pts',(108.351518755967,-4.30568555138091,329.992850279468));
#70636=CARTESIAN_POINT('Ctrl Pts',(108.073280721693,-6.54067253488663,335.91108681396));
#70637=CARTESIAN_POINT('Ctrl Pts',(107.795042687419,-2.77338087329526,340.993232426899));
#70638=CARTESIAN_POINT('Ctrl Pts',(107.516804653145,3.53900148068459,340.575477101639));
#70639=CARTESIAN_POINT('Ctrl Pts',(107.238566618871,6.60369441141642,335.041188734113));
#70640=CARTESIAN_POINT('Ctrl Pts',(106.960328584597,3.60827445116114,329.469102073235));
#70641=CARTESIAN_POINT('Ctrl Pts',(106.682090550323,-2.69840571488112,328.972638803831));
#70642=CARTESIAN_POINT('Ctrl Pts',(106.403852516049,-6.52879878478004,334.007395940445));
#70643=CARTESIAN_POINT('Ctrl Pts',(106.125614481775,-4.36780957479843,339.953051171701));
#70644=CARTESIAN_POINT('Ctrl Pts',(105.847376447501,1.80145401321206,341.353364449603));
#70645=CARTESIAN_POINT('Ctrl Pts',(105.569138413227,6.31754984271549,336.923288947608));
#70646=CARTESIAN_POINT('Ctrl Pts',(105.290900378953,5.03612342844174,330.728239566094));
#70647=CARTESIAN_POINT('Ctrl Pts',(105.012662344679,-0.866879123053034,
328.453321683692));
#70648=CARTESIAN_POINT('Ctrl Pts',(104.734424310405,-5.97435949843692,332.186193863354));
#70649=CARTESIAN_POINT('Ctrl Pts',(104.456186276131,-5.5992583435069,338.501254402905));
#70650=CARTESIAN_POINT('Ctrl Pts',(104.177948241857,-0.0858004516582664,
341.60326545534));
#70651=CARTESIAN_POINT('Ctrl Pts',(103.899710207583,5.50639524826456,338.645557263449));
#70652=CARTESIAN_POINT('Ctrl Pts',(103.62147217331,6.04545330311564,332.342374979226));
#70653=CARTESIAN_POINT('Ctrl Pts',(103.343234139036,1.03668809244208,328.478055950089));
#70654=CARTESIAN_POINT('Ctrl Pts',(103.064996104762,-4.9234304791743,330.598828711817));
#70655=CARTESIAN_POINT('Ctrl Pts',(102.786758070488,-6.36538956976742,336.758491403529));
#70656=CARTESIAN_POINT('Ctrl Pts',(102.508520036214,-1.96592460518105,341.304412489514));
#70657=CARTESIAN_POINT('Ctrl Pts',(102.23028200194,4.23764035258036,340.064867286846));
#70658=CARTESIAN_POINT('Ctrl Pts',(101.952043967666,6.55238530624785,334.17736813236));
#70659=CARTESIAN_POINT('Ctrl Pts',(101.673805933392,2.85410297742028,329.044786100778));
#70660=CARTESIAN_POINT('Ctrl Pts',(101.395567899118,-3.46334752729499,329.377215965702));
#70661=CARTESIAN_POINT('Ctrl Pts',(101.117329864844,-6.60253512513736,334.869591746742));
#70662=CARTESIAN_POINT('Ctrl Pts',(100.83909183057,-3.68267369189987,340.481641256976));
#70663=CARTESIAN_POINT('Ctrl Pts',(100.560853796296,2.61672303221954,341.063269494575));
#70664=CARTESIAN_POINT('Ctrl Pts',(100.282615762022,6.51479165243972,336.080724810714));
#70665=CARTESIAN_POINT('Ctrl Pts',(100.004377727748,4.43433213138313,330.106414919533));
#70666=CARTESIAN_POINT('Ctrl Pts',(99.726139693474,-1.71544853600877,328.622875827498));
#70667=CARTESIAN_POINT('Ctrl Pts',(99.4479016591999,-6.29098740188432,332.991529462371));
#70668=CARTESIAN_POINT('Ctrl Pts',(99.169663624926,-5.09337998387248,339.203326864648));
#70669=CARTESIAN_POINT('Ctrl Pts',(98.8914255906521,0.778347067173814,341.557793244242));
#70670=CARTESIAN_POINT('Ctrl Pts',(98.6131875563781,5.93579650305857,337.894269556463));
#70671=CARTESIAN_POINT('Ctrl Pts',(98.3349495221042,5.64605310029925,331.574717416068));
#70672=CARTESIAN_POINT('Ctrl Pts',(98.0567114878303,0.175010103002464,328.398496545858));
#70673=CARTESIAN_POINT('Ctrl Pts',(97.7784734535562,-5.4566370826748,331.280377957486));
#70674=CARTESIAN_POINT('Ctrl Pts',(97.5002354192825,-6.08080895741272,337.575701615994));
#70675=CARTESIAN_POINT('Ctrl Pts',(97.2219973850083,-1.12471220452607,341.507341918801));
#70676=CARTESIAN_POINT('Ctrl Pts',(96.9437593507347,4.86351633772921,339.467290590932));
#70677=CARTESIAN_POINT('Ctrl Pts',(96.6655213164605,6.38856772223389,333.327672624866));
#70678=CARTESIAN_POINT('Ctrl Pts',(96.3872832821866,2.05092480314952,328.722724807449));
#70679=CARTESIAN_POINT('Ctrl Pts',(96.1090452479129,-4.16882153618468,329.878339781806));
#70680=CARTESIAN_POINT('Ctrl Pts',(95.8308072136387,-6.56290188346721,335.734026742819));
#70681=CARTESIAN_POINT('Ctrl Pts',(95.5525691793649,-2.9343040405649,340.916108196163));
#70682=CARTESIAN_POINT('Ctrl Pts',(95.2743311450908,3.38706131010718,340.669064479504));
#70683=CARTESIAN_POINT('Ctrl Pts',(94.996093110817,6.60017048943689,335.219603965257));
#70684=CARTESIAN_POINT('Ctrl Pts',(94.7178550765429,3.75640062896709,329.568616133444));
#70685=CARTESIAN_POINT('Ctrl Pts',(94.4396170422691,-2.5345626443234,328.901929108874));
#70686=CARTESIAN_POINT('Ctrl Pts',(94.161379007995,-6.49959518900162,333.831351733713));
#70687=CARTESIAN_POINT('Ctrl Pts',(93.8831409737213,-4.5000451626008,339.833225623302));
#70688=CARTESIAN_POINT('Ctrl Pts',(93.6049029394472,1.62912988896106,341.399719696681));
#70689=CARTESIAN_POINT('Ctrl Pts',(93.3266649051734,6.26327648734109,337.093285464125));
#70690=CARTESIAN_POINT('Ctrl Pts',(93.0484268708992,5.14970669909762,330.865874057982));
#70691=CARTESIAN_POINT('Ctrl Pts',(92.7701888366256,-0.689672917361457,
328.432289009233));
#70692=CARTESIAN_POINT('Ctrl Pts',(92.4919508023513,-5.89614987711338,332.025795397454));
#70693=CARTESIAN_POINT('Ctrl Pts',(92.2137127680778,-5.69181712166809,338.348685450244));
#70694=CARTESIAN_POINT('Ctrl Pts',(91.9354747338034,-0.264187804751184,
341.598536291861));
#70695=CARTESIAN_POINT('Ctrl Pts',(91.6572366995299,5.4058827611804,338.793007772674));
#70696=CARTESIAN_POINT('Ctrl Pts',(91.3789986652556,6.11505450787548,332.506692005207));
#70697=CARTESIAN_POINT('Ctrl Pts',(91.1007606309819,1.21253099074983,328.508448183395));
#70698=CARTESIAN_POINT('Ctrl Pts',(90.8225225967078,-4.80271431965887,330.467405648535));
#70699=CARTESIAN_POINT('Ctrl Pts',(90.544284562434,-6.41057958686376,336.58585804903));
#70700=CARTESIAN_POINT('Ctrl Pts',(90.26604652816,-2.1355505872034,341.248991925158));
#70701=CARTESIAN_POINT('Ctrl Pts',(89.9878084938861,4.09924166565854,340.177518146537));
#70702=CARTESIAN_POINT('Ctrl Pts',(89.7095704596121,6.57222034665343,334.354712384882));
#70703=CARTESIAN_POINT('Ctrl Pts',(89.4313324253382,3.01396942133779,329.124077543191));
#70704=CARTESIAN_POINT('Ctrl Pts',(89.1530943910642,-3.31015675582382,329.285690011641));
#70705=CARTESIAN_POINT('Ctrl Pts',(88.8748563567904,-6.59660093599952,334.69124041333));
#70706=CARTESIAN_POINT('Ctrl Pts',(88.5966183225163,-3.82944180287868,340.380134930423));
#70707=CARTESIAN_POINT('Ctrl Pts',(88.3183802882425,2.45193955027557,341.131759032528));
#70708=CARTESIAN_POINT('Ctrl Pts',(88.0401422539686,6.48321216871036,336.256358375097));
#70709=CARTESIAN_POINT('Ctrl Pts',(87.7619042196945,4.56493667197442,330.228016180658));
#70710=CARTESIAN_POINT('Ctrl Pts',(87.4836661854207,-1.54251383027763,328.578853102865));
#70711=CARTESIAN_POINT('Ctrl Pts',(87.2054281511466,-6.23442215795071,332.822281756599));
#70712=CARTESIAN_POINT('Ctrl Pts',(86.9271901168728,-5.20509329119263,339.064170299233));
#70713=CARTESIAN_POINT('Ctrl Pts',(86.6489520825988,0.600872861841872,341.576429745317));
#70714=CARTESIAN_POINT('Ctrl Pts',(86.3707140483249,5.855426858433,338.053596682067));
#70715=CARTESIAN_POINT('Ctrl Pts',(86.092476014051,5.73654205299892,331.728523014697));
#70716=CARTESIAN_POINT('Ctrl Pts',(85.8142379797769,0.353317276749643,328.405635489819));
#70717=CARTESIAN_POINT('Ctrl Pts',(85.535999945503,-5.35414154941832,331.134298943272));
#70718=CARTESIAN_POINT('Ctrl Pts',(85.2577619112292,-6.14818370268483,337.410459198831));
#70719=CARTESIAN_POINT('Ctrl Pts',(84.9795238769551,-1.30012841904015,341.474576625942));
#70720=CARTESIAN_POINT('Ctrl Pts',(84.7012858426813,4.74103552489365,339.597070648021));
#70721=CARTESIAN_POINT('Ctrl Pts',(84.4230478084072,6.43142114520221,333.500900789061));
#70722=CARTESIAN_POINT('Ctrl Pts',(84.1448097741333,2.21978650817918,328.780432149313));
#70723=CARTESIAN_POINT('Ctrl Pts',(83.8665717398596,-4.02891344340471,329.767569125469));
#70724=CARTESIAN_POINT('Ctrl Pts',(83.5883337055854,-6.58033899464105,335.556430684628));
#70725=CARTESIAN_POINT('Ctrl Pts',(83.3100956713115,-3.09308457613965,340.834664017408));
#70726=CARTESIAN_POINT('Ctrl Pts',(83.0318576370376,3.2326479040316,340.758512300912));
#70727=CARTESIAN_POINT('Ctrl Pts',(82.7536196027636,6.5918271164779,335.397858841371));
#70728=CARTESIAN_POINT('Ctrl Pts',(82.4753815684898,3.90178387934119,329.67209619549));
#70729=CARTESIAN_POINT('Ctrl Pts',(82.1971435342158,-2.36886883363129,328.835672231278));
#70730=CARTESIAN_POINT('Ctrl Pts',(81.918905499942,-6.46564558242699,333.656160875092));
#70731=CARTESIAN_POINT('Ctrl Pts',(81.6406674656679,-4.62899481300182,339.709870848802));
#70732=CARTESIAN_POINT('Ctrl Pts',(81.3624294313939,1.45561617246357,341.441401862146));
#70733=CARTESIAN_POINT('Ctrl Pts',(81.0841913971202,6.20442968131859,337.261753461534));
#70734=CARTESIAN_POINT('Ctrl Pts',(80.8059533628462,5.25952964885982,331.006527292699));
#70735=CARTESIAN_POINT('Ctrl Pts',(80.5277153285721,-0.511963111827283,
328.416052083794));
#70736=CARTESIAN_POINT('Ctrl Pts',(80.2494772942983,-5.81363488135362,331.867568698678));
#70737=CARTESIAN_POINT('Ctrl Pts',(79.9712392600242,-5.78021972937194,338.193671284176));
#70738=CARTESIAN_POINT('Ctrl Pts',(79.6930012257504,-0.442382247648974,
341.588988870696));
#70739=CARTESIAN_POINT('Ctrl Pts',(79.4147631914764,5.30142289319017,338.937688623895));
#70740=CARTESIAN_POINT('Ctrl Pts',(79.1365251572024,6.18019049382234,332.672829647134));
#70741=CARTESIAN_POINT('Ctrl Pts',(78.8582871229286,1.38748849773591,328.54358055422));
#70742=CARTESIAN_POINT('Ctrl Pts',(78.5800490886545,-4.67849121342611,330.339292290103));
#70743=CARTESIAN_POINT('Ctrl Pts',(78.3018110543807,-6.4510885924441,336.412066699426));
#70744=CARTESIAN_POINT('Ctrl Pts',(78.0235730201066,-2.30361718808769,341.189008340755));
#70745=CARTESIAN_POINT('Ctrl Pts',(77.7453349858328,3.95784970844284,340.286388377386));
#70746=CARTESIAN_POINT('Ctrl Pts',(77.4670969515588,6.58725634530131,334.532527827055));
#70747=CARTESIAN_POINT('Ctrl Pts',(77.1888589172849,3.17163506182105,329.207659589957));
#70748=CARTESIAN_POINT('Ctrl Pts',(76.910620883011,-3.15454890463561,329.198336652351));
#70749=CARTESIAN_POINT('Ctrl Pts',(76.6323828487369,-6.58584990237367,334.513114536472));
#70750=CARTESIAN_POINT('Ctrl Pts',(76.3541448144631,-3.97341365168864,340.274700024055));
#70751=CARTESIAN_POINT('Ctrl Pts',(76.0759067801891,2.2853656596617,341.195771154007));
#70752=CARTESIAN_POINT('Ctrl Pts',(75.7976687459152,6.44689863708233,336.431074545359));
#70753=CARTESIAN_POINT('Ctrl Pts',(75.5194307116413,4.69220789132043,330.353101949061));
#70754=CARTESIAN_POINT('Ctrl Pts',(75.2411926773673,-1.3684527794313,328.539519106006));
#70755=CARTESIAN_POINT('Ctrl Pts',(74.9629546430933,-6.17330453282882,332.654624222828));
#70756=CARTESIAN_POINT('Ctrl Pts',(74.6847166088195,-5.31300583427489,338.92204607267));
#70757=CARTESIAN_POINT('Ctrl Pts',(74.4064785745454,0.422959898555554,341.590264130928));
#70758=CARTESIAN_POINT('Ctrl Pts',(74.1282405402716,5.77078157535943,338.210694068373));
#70759=CARTESIAN_POINT('Ctrl Pts',(73.8500025059976,5.82284217705239,331.884717449037));
#70760=CARTESIAN_POINT('Ctrl Pts',(73.5717644717237,0.531366457874022,328.417589645226));
#70761=CARTESIAN_POINT('Ctrl Pts',(73.2935264374498,-5.24773641673927,330.991042667773));
#70762=CARTESIAN_POINT('Ctrl Pts',(73.0152884031758,-6.21106903817348,337.243456661992));
#70763=CARTESIAN_POINT('Ctrl Pts',(72.7370503689018,-1.47459527850462,341.437083590866));
#70764=CARTESIAN_POINT('Ctrl Pts',(72.4588123346279,4.61509280325731,339.723493919602));
#70765=CARTESIAN_POINT('Ctrl Pts',(72.180574300354,6.46957833812812,333.675223596974));
#70766=CARTESIAN_POINT('Ctrl Pts',(71.90233626608,2.3870273229185,328.842681025737));
#70767=CARTESIAN_POINT('Ctrl Pts',(71.6240982318062,-3.88606343406789,329.660619195301));
#70768=CARTESIAN_POINT('Ctrl Pts',(71.3458601975322,-6.59297113581244,335.378428320206));
#70769=CARTESIAN_POINT('Ctrl Pts',(71.0676221632582,-3.24960653831636,340.748959361252));
#70770=CARTESIAN_POINT('Ctrl Pts',(70.7893841289843,3.07587401527876,340.843755250977));
#70771=CARTESIAN_POINT('Ctrl Pts',(70.5111460947104,6.57867038487854,335.575823200567));
#70772=CARTESIAN_POINT('Ctrl Pts',(70.2329080604365,4.04431804329124,329.779466698133));
#70773=CARTESIAN_POINT('Ctrl Pts',(69.9546700261624,-2.20144527258785,328.773916551877));
#70774=CARTESIAN_POINT('Ctrl Pts',(69.6764319918886,-6.42697475509217,333.481951289123));
#70775=CARTESIAN_POINT('Ctrl Pts',(69.3981939576146,-4.75456436684029,339.583076921977));
#70776=CARTESIAN_POINT('Ctrl Pts',(69.1199559233406,1.28103956360592,341.478380509639));
#70777=CARTESIAN_POINT('Ctrl Pts',(68.8417178890667,6.14105239464392,337.428569924345));
#70778=CARTESIAN_POINT('Ctrl Pts',(68.5634798547928,5.36551208490198,331.150096565112));
#70779=CARTESIAN_POINT('Ctrl Pts',(68.2852418205188,-0.333879470325961,
328.404622763596));
#70780=CARTESIAN_POINT('Ctrl Pts',(68.007003786245,-5.72687476368866,331.711629304318));
#70781=CARTESIAN_POINT('Ctrl Pts',(67.728765751971,-5.86440161494724,338.036325096198));
#70782=CARTESIAN_POINT('Ctrl Pts',(67.450527717697,-0.620253662594679,341.574630163379));
#70783=CARTESIAN_POINT('Ctrl Pts',(67.1722896834231,5.19309192099196,339.079494171012));
#70784=CARTESIAN_POINT('Ctrl Pts',(66.8940516491492,6.24081369859539,332.840666591141));
#70785=CARTESIAN_POINT('Ctrl Pts',(66.6158136148752,1.56143285925702,328.583427408871));
#70786=CARTESIAN_POINT('Ctrl Pts',(66.3375755806014,-4.55085186831029,330.214582185024));
#70787=CARTESIAN_POINT('Ctrl Pts',(66.0593375463273,-6.48688700679271,336.237244257329));
#70788=CARTESIAN_POINT('Ctrl Pts',(65.7810995120535,-2.47000168543674,341.124505536378));
#70789=CARTESIAN_POINT('Ctrl Pts',(65.5028614777794,3.81356772547941,340.391398482247));
#70790=CARTESIAN_POINT('Ctrl Pts',(65.2246234435056,6.59748232289047,334.710684617869));
#70791=CARTESIAN_POINT('Ctrl Pts',(64.9463854092316,3.32698477126441,329.295471209385));
#70792=CARTESIAN_POINT('Ctrl Pts',(64.6681473749577,-2.99663759873627,329.115219673341));
#70793=CARTESIAN_POINT('Ctrl Pts',(64.3899093406837,-6.57028987467513,334.335344183859));
#70794=CARTESIAN_POINT('Ctrl Pts',(64.1116713064098,-4.1144841099442,340.165413526544));
#70795=CARTESIAN_POINT('Ctrl Pts',(63.8334332721358,2.1171229927966,341.255259117299));
#70796=CARTESIAN_POINT('Ctrl Pts',(63.5551952378619,6.40587757373213,336.604745743583));
#70797=CARTESIAN_POINT('Ctrl Pts',(63.2769572035879,4.81605285585167,330.481580886987));
#70798=CARTESIAN_POINT('Ctrl Pts',(62.9987191693141,-1.19339248302022,328.504902558648));
#70799=CARTESIAN_POINT('Ctrl Pts',(62.72048113504,-6.10767915466864,332.488679284755));
#70800=CARTESIAN_POINT('Ctrl Pts',(62.4422431007662,-5.41703881527419,338.777057964211));
#70801=CARTESIAN_POINT('Ctrl Pts',(62.1640050664922,0.244738089535523,341.599286299194));
#70802=CARTESIAN_POINT('Ctrl Pts',(61.8857670322182,5.68192246190678,338.365447002713));
#70803=CARTESIAN_POINT('Ctrl Pts',(61.6075289979444,5.90489045602424,332.043186665759));
#70804=CARTESIAN_POINT('Ctrl Pts',(61.3292909636703,0.709027634688525,328.434350283145));
#70805=CARTESIAN_POINT('Ctrl Pts',(61.0510529293965,-5.13749938177011,330.850713736857));
#70806=CARTESIAN_POINT('Ctrl Pts',(60.7728148951225,-6.2694190449449,337.074815950891));
#70807=CARTESIAN_POINT('Ctrl Pts',(60.4945768608485,-1.64798538704716,341.394890191025));
#70808=CARTESIAN_POINT('Ctrl Pts',(60.2163388265747,4.48578013631931,339.84646809128));
#70809=CARTESIAN_POINT('Ctrl Pts',(59.9381007923006,6.50301143859184,333.850513757919));
#70810=CARTESIAN_POINT('Ctrl Pts',(59.6598627580269,2.5525251279602,328.909425982527));
#70811=CARTESIAN_POINT('Ctrl Pts',(59.3816247237527,-3.7403758173912,329.557568086244));
#70812=CARTESIAN_POINT('Ctrl Pts',(59.103386689479,-6.60078908297948,335.200149627053));
#70813=CARTESIAN_POINT('Ctrl Pts',(58.8251486552049,-3.4037556346047,340.659056809318));
#70814=CARTESIAN_POINT('Ctrl Pts',(58.5469106209311,2.91685412029599,340.924731085214));
#70815=CARTESIAN_POINT('Ctrl Pts',(58.2686725866571,6.56070990169731,335.753367093097));
#70816=CARTESIAN_POINT('Ctrl Pts',(57.9904345523832,4.18389904223041,329.890649239325));
#70817=CARTESIAN_POINT('Ctrl Pts',(57.7121965181092,-2.03241421404269,328.716707164732));
#70818=CARTESIAN_POINT('Ctrl Pts',(57.4339584838352,-6.38361094447344,333.308850183812));
#70819=CARTESIAN_POINT('Ctrl Pts',(57.1557204495613,-4.87666213310401,339.452936427881));
#70820=CARTESIAN_POINT('Ctrl Pts',(56.8774824152874,1.10552753839988,341.510628637314));
#70821=CARTESIAN_POINT('Ctrl Pts',(56.5992443810134,6.07319090547391,337.593613043008));
#70822=CARTESIAN_POINT('Ctrl Pts',(56.3210063467396,5.46757661874537,331.296477040796));
#70823=CARTESIAN_POINT('Ctrl Pts',(56.0427683124655,-0.155552029707196,
328.398009394339));
#70824=CARTESIAN_POINT('Ctrl Pts',(55.7645302781917,-5.63593287644166,331.558091081473));
#70825=CARTESIAN_POINT('Ctrl Pts',(55.4862922439177,-5.94430130869852,337.876761780648));
#70826=CARTESIAN_POINT('Ctrl Pts',(55.2080542096437,-0.797672167706236,
341.555470654657));
#70827=CARTESIAN_POINT('Ctrl Pts',(54.9298161753698,5.08096894796816,339.218320867475));
#70828=CARTESIAN_POINT('Ctrl Pts',(54.6515781410958,6.29687985507091,333.010080282526));
#70829=CARTESIAN_POINT('Ctrl Pts',(54.373340106822,1.73423706096941,328.627959651136));
#70830=CARTESIAN_POINT('Ctrl Pts',(54.0951020725479,-4.41988948668667,330.093366396737));
#70831=CARTESIAN_POINT('Ctrl Pts',(53.8168640382742,-6.51794868987227,336.06151837826));
#70832=CARTESIAN_POINT('Ctrl Pts',(53.5386260040001,-2.63458258512705,341.055530612038));
#70833=CARTESIAN_POINT('Ctrl Pts',(53.2603879697263,3.66650107161404,340.492471782635));
#70834=CARTESIAN_POINT('Ctrl Pts',(52.9821499354522,6.60289081240205,334.889052667058));
#70835=CARTESIAN_POINT('Ctrl Pts',(52.7039119011784,3.47990511315732,329.387448281342));
#70836=CARTESIAN_POINT('Ctrl Pts',(52.4256738669043,-2.83653814511659,329.036399766711));
#70837=CARTESIAN_POINT('Ctrl Pts',(52.1474358326305,-6.54993221485141,334.158059163574));
#70838=CARTESIAN_POINT('Ctrl Pts',(51.8691977983565,-4.25255016785809,340.052355238999));
#70839=CARTESIAN_POINT('Ctrl Pts',(51.5909597640826,1.947334400641,341.310179484236));
#70840=CARTESIAN_POINT('Ctrl Pts',(51.3127217298086,6.36017893228049,336.777245154886));
#70841=CARTESIAN_POINT('Ctrl Pts',(51.0344836955347,4.93638113385334,330.613359178993));
#70842=CARTESIAN_POINT('Ctrl Pts',(50.7562456612607,-1.01746077024492,328.475028737825));
#70843=CARTESIAN_POINT('Ctrl Pts',(50.4780076269868,-6.03759394318577,332.324568115538));
#70844=CARTESIAN_POINT('Ctrl Pts',(50.1997695927128,-5.51711626920556,338.629311844311));
#70845=CARTESIAN_POINT('Ctrl Pts',(49.9215315584389,0.0663375725219412,
341.603489662116));
#70846=CARTESIAN_POINT('Ctrl Pts',(49.643293524165,5.58891440308703,338.517742484343));
#70847=CARTESIAN_POINT('Ctrl Pts',(49.3650554898911,5.98262697818051,332.203814950485));
#70848=CARTESIAN_POINT('Ctrl Pts',(49.0868174556171,0.886171078827202,328.455905164941));
#70849=CARTESIAN_POINT('Ctrl Pts',(48.8085794213432,-5.02351093970216,330.713414618851));
#70850=CARTESIAN_POINT('Ctrl Pts',(48.5303413870692,-6.32319111576674,336.904660207144));
#70851=CARTESIAN_POINT('Ctrl Pts',(48.2521033527954,-1.82017213504033,341.348027236081));
#70852=CARTESIAN_POINT('Ctrl Pts',(47.9738653185213,4.35319194831591,339.965903367194));
#70853=CARTESIAN_POINT('Ctrl Pts',(47.6956272842475,6.53169603371061,334.026643274848));
#70854=CARTESIAN_POINT('Ctrl Pts',(47.4173892499734,2.7161590766445,328.980618282452));
#70855=CARTESIAN_POINT('Ctrl Pts',(47.1391512156996,-3.591956974616,329.458491046321));
#70856=CARTESIAN_POINT('Ctrl Pts',(46.8609131814255,-6.60378712746943,335.021724784445));
#70857=CARTESIAN_POINT('Ctrl Pts',(46.5826751471518,-3.55541930518241,340.565022008539));
#70858=CARTESIAN_POINT('Ctrl Pts',(46.3044371128777,2.75570433556762,341.001380674989));
#70859=CARTESIAN_POINT('Ctrl Pts',(46.0261990786039,6.53795878169654,335.930360876233));
#70860=CARTESIAN_POINT('Ctrl Pts',(45.7479610443298,4.320424953976,330.005562633464));
#70861=CARTESIAN_POINT('Ctrl Pts',(45.4697230100559,-1.86189908464054,328.664085844189));
#70862=CARTESIAN_POINT('Ctrl Pts',(45.191484975782,-6.33558581486789,333.136983957762));
#70863=CARTESIAN_POINT('Ctrl Pts',(44.9132469415081,-4.99519895588432,339.319544395225));
#70864=CARTESIAN_POINT('Ctrl Pts',(44.6350089072341,0.929208255898556,341.538122697561));
#70865=CARTESIAN_POINT('Ctrl Pts',(44.3567708729602,6.0008947663347,337.756762302877));
#70866=CARTESIAN_POINT('Ctrl Pts',(44.0785328386862,5.56564872276705,331.445561832588));
#70867=CARTESIAN_POINT('Ctrl Pts',(43.8002948044123,0.0228889951565719,
328.396216805112));
#70868=CARTESIAN_POINT('Ctrl Pts',(43.5220567701384,-5.54087562546809,331.407066143903));
#70869=CARTESIAN_POINT('Ctrl Pts',(43.2438187358644,-6.01986046779084,337.715097850819));
#70870=CARTESIAN_POINT('Ctrl Pts',(42.9655807015905,-0.974508211817014,
341.531524334815));
#70871=CARTESIAN_POINT('Ctrl Pts',(42.6873426673165,4.96513584642345,339.354067341895));
#70872=CARTESIAN_POINT('Ctrl Pts',(42.4091046330427,6.34834802368656,333.180947015245));
#70873=CARTESIAN_POINT('Ctrl Pts',(42.1308665987686,1.9057749210758,328.677144763527));
#70874=CARTESIAN_POINT('Ctrl Pts',(41.8526285644948,-4.28569969741449,329.97573343713));
#70875=CARTESIAN_POINT('Ctrl Pts',(41.5743905302207,-6.54425096041135,335.885017377426));
#70876=CARTESIAN_POINT('Ctrl Pts',(41.2961524959469,-2.79723971002455,340.982133933291));
#70877=CARTESIAN_POINT('Ctrl Pts',(41.0179144616729,3.51675713506133,340.58953447473));
#70878=CARTESIAN_POINT('Ctrl Pts',(40.7396764273991,6.60347786455166,335.0675017301));
#70879=CARTESIAN_POINT('Ctrl Pts',(40.461438393125,3.63028442491644,329.483523644082));
#70880=CARTESIAN_POINT('Ctrl Pts',(40.1832003588512,-2.67436744855432,328.961934486832));
#70881=CARTESIAN_POINT('Ctrl Pts',(39.9049623245772,-6.52479178808562,333.981388929316));
#70882=CARTESIAN_POINT('Ctrl Pts',(39.6267242903033,-4.38751100945966,339.935607716691));
#70883=CARTESIAN_POINT('Ctrl Pts',(39.3484862560292,1.77612386299106,341.36049215191));
#70884=CARTESIAN_POINT('Ctrl Pts',(39.0702482217554,6.30983608192015,336.948446820032));
#70885=CARTESIAN_POINT('Ctrl Pts',(38.7920101874814,5.05310486149901,330.748340600438));
#70886=CARTESIAN_POINT('Ctrl Pts',(38.5137721532075,-0.840786106614272,
328.449919457434));
#70887=CARTESIAN_POINT('Ctrl Pts',(38.2355341189336,-5.96310007467022,332.162410549312));
#70888=CARTESIAN_POINT('Ctrl Pts',(37.9572960846596,-5.61316511941414,338.478915597335));
#70889=CARTESIAN_POINT('Ctrl Pts',(37.6790580503857,-0.11211138425306,341.602871150394));
#70890=CARTESIAN_POINT('Ctrl Pts',(37.4008200161118,5.49182531347575,338.667469306956));
#70891=CARTESIAN_POINT('Ctrl Pts',(37.1225819818378,6.05599498023661,332.366485012281));
#70892=CARTESIAN_POINT('Ctrl Pts',(36.8443439475639,1.06266743997372,328.48223855122));
#70893=CARTESIAN_POINT('Ctrl Pts',(36.5661059132899,-4.90585432500734,330.579245569702));
#70894=CARTESIAN_POINT('Ctrl Pts',(36.287867879016,-6.37234598622031,336.733113678641));
#70895=CARTESIAN_POINT('Ctrl Pts',(36.009629844742,-1.99102979155148,341.296528945406));
#70896=CARTESIAN_POINT('Ctrl Pts',(35.7313918104681,4.21742505527259,340.081712535589));
#70897=CARTESIAN_POINT('Ctrl Pts',(35.4531537761941,6.55561117796478,334.203483537813));
#70898=CARTESIAN_POINT('Ctrl Pts',(35.1749157419203,2.87780968330108,329.056205940826));
#70899=CARTESIAN_POINT('Ctrl Pts',(34.8966777076463,-3.44091528132674,329.363460421683));
#70900=CARTESIAN_POINT('Ctrl Pts',(34.6184396733724,-6.6019630801073,334.843284078378));
#70901=CARTESIAN_POINT('Ctrl Pts',(34.3402016390984,-3.70448680508874,340.466923623218));
#70902=CARTESIAN_POINT('Ctrl Pts',(34.0619636048245,2.59254233282417,341.073648050696));
#70903=CARTESIAN_POINT('Ctrl Pts',(33.7837255705505,6.51043363776641,336.106675308945));
#70904=CARTESIAN_POINT('Ctrl Pts',(33.5054875362766,4.45379608717343,330.124122970679));
#70905=CARTESIAN_POINT('Ctrl Pts',(33.2272495020026,-1.69002439469614,328.616091014393));
#70906=CARTESIAN_POINT('Ctrl Pts',(32.9490114677288,-6.28293443427222,332.966478107856));
#70907=CARTESIAN_POINT('Ctrl Pts',(32.6707734334547,-5.11008827947693,339.182998227008));
#70908=CARTESIAN_POINT('Ctrl Pts',(32.3925353991809,0.752210464614984,341.560842614186));
#70909=CARTESIAN_POINT('Ctrl Pts',(32.1142973649069,5.92421676793797,337.917898572204));
#70910=CARTESIAN_POINT('Ctrl Pts',(31.836059330633,5.65965678462045,331.597242078624));
#70911=CARTESIAN_POINT('Ctrl Pts',(31.557821296359,0.201313306453949,328.399246304865));
#70912=CARTESIAN_POINT('Ctrl Pts',(31.2795832620851,-5.44177242166582,331.258664770167));
#70913=CARTESIAN_POINT('Ctrl Pts',(31.0013452278111,-6.09102391885213,337.551451353869));
#70914=CARTESIAN_POINT('Ctrl Pts',(30.7231071935373,-1.15063266907353,341.502808689487));
#70915=CARTESIAN_POINT('Ctrl Pts',(30.4448691592632,4.8456771978035,339.486634472059));
#70916=CARTESIAN_POINT('Ctrl Pts',(30.1666311249894,6.39518062233446,333.353142022241));
#70917=CARTESIAN_POINT('Ctrl Pts',(29.8883930907154,2.07592118246034,328.730946831028));
#70918=CARTESIAN_POINT('Ctrl Pts',(29.6101550564415,-4.14838048601121,329.861769201907));
#70919=CARTESIAN_POINT('Ctrl Pts',(29.3319170221675,-6.56577461246588,335.707870136034));
#70920=CARTESIAN_POINT('Ctrl Pts',(29.0536789878936,-2.95785428773503,340.904369094469));
#70921=CARTESIAN_POINT('Ctrl Pts',(28.7754409536196,3.36444525899253,340.682515683255));
#70922=CARTESIAN_POINT('Ctrl Pts',(28.4972029193457,6.59924305067326,335.245901503312));
#70923=CARTESIAN_POINT('Ctrl Pts',(28.2189648850717,3.77801289941892,329.58362714328));
#70924=CARTESIAN_POINT('Ctrl Pts',(27.9407268507979,-2.51024392625319,328.891878208328));
#70925=CARTESIAN_POINT('Ctrl Pts',(27.6624888165239,-6.49488695194235,333.805462485863));
#70926=CARTESIAN_POINT('Ctrl Pts',(27.38425078225,-4.51926808620829,339.815256208777));
#70927=CARTESIAN_POINT('Ctrl Pts',(27.106012747976,1.60361639795151,341.406160381961));
#70928=CARTESIAN_POINT('Ctrl Pts',(26.8277747137021,6.25488578305044,337.118225727392));
#70929=CARTESIAN_POINT('Ctrl Pts',(26.5495366794281,5.16613880700681,330.886426587756));
#70930=CARTESIAN_POINT('Ctrl Pts',(26.2712986451542,-0.663497500143172,
328.429593052291));
#70931=CARTESIAN_POINT('Ctrl Pts',(25.9930606108802,-5.88425194461882,332.002324993692));
#70932=CARTESIAN_POINT('Ctrl Pts',(25.7148225766064,-5.70511523093411,338.325979042772));
#70933=CARTESIAN_POINT('Ctrl Pts',(25.4365845423323,-0.290478477183944,
341.597431215669));
#70934=CARTESIAN_POINT('Ctrl Pts',(25.1583465080585,5.39072608762264,338.814518139873));
#70935=CARTESIAN_POINT('Ctrl Pts',(24.8801084737845,6.12494088880454,332.53107806931));
#70936=CARTESIAN_POINT('Ctrl Pts',(24.6018704395106,1.23838784030986,328.513331213315));
#70937=CARTESIAN_POINT('Ctrl Pts',(24.3236324052366,-4.78461545066262,330.448304559785));
#70938=CARTESIAN_POINT('Ctrl Pts',(24.0453943709627,-6.41684776337031,336.560301628827));
#70939=CARTESIAN_POINT('Ctrl Pts',(23.7671563366888,-2.16043359615079,341.240432923108));
#70940=CARTESIAN_POINT('Ctrl Pts',(23.4889183024148,4.0785785943087,340.193811032492));
#70941=CARTESIAN_POINT('Ctrl Pts',(23.2106802681409,6.57473940849246,334.380905417883));
#70942=CARTESIAN_POINT('Ctrl Pts',(22.9324422338669,3.03735891049729,329.136133763461));
#70943=CARTESIAN_POINT('Ctrl Pts',(22.654204199593,-3.28736102831721,329.272545603789));
#70944=CARTESIAN_POINT('Ctrl Pts',(22.3759661653191,-6.59531827281427,334.664957806429));
#70945=CARTESIAN_POINT('Ctrl Pts',(22.0977281310451,-3.85084928508779,340.364833284896));
#70946=CARTESIAN_POINT('Ctrl Pts',(21.8194900967712,2.42748725312145,341.141480442623));
#70947=CARTESIAN_POINT('Ctrl Pts',(21.5412520624972,6.47815456879428,336.282181646259));
#70948=CARTESIAN_POINT('Ctrl Pts',(21.2630140282234,4.58391505408935,330.246243678092));
#70949=CARTESIAN_POINT('Ctrl Pts',(20.9847759939494,-1.5169156472776,328.572757721213));
#70950=CARTESIAN_POINT('Ctrl Pts',(20.7065379596755,-6.22569524877642,332.797457137636));
#70951=CARTESIAN_POINT('Ctrl Pts',(20.4282999254015,-5.22124621158455,339.043397629371));
#70952=CARTESIAN_POINT('Ctrl Pts',(20.1500618911275,0.574663408510707,341.578771797085));
#70953=CARTESIAN_POINT('Ctrl Pts',(19.8718238568537,5.8432129006337,338.076904189125));
#70954=CARTESIAN_POINT('Ctrl Pts',(19.5935858225797,5.74953215952618,331.751407021838));
#70955=CARTESIAN_POINT('Ctrl Pts',(19.3153477883058,0.379590618577057,328.407095681455));
#70956=CARTESIAN_POINT('Ctrl Pts',(19.0371097540318,-5.33869563029188,331.112995323094));
#70957=CARTESIAN_POINT('Ctrl Pts',(18.7588717197579,-6.1577396982603,337.385941784633));
#70958=CARTESIAN_POINT('Ctrl Pts',(18.4806336854839,-1.3259169332242,341.469344686858));
#70959=CARTESIAN_POINT('Ctrl Pts',(18.20239565121,4.7226802309299,339.615925457325));
#70960=CARTESIAN_POINT('Ctrl Pts',(17.924157616936,6.43734345380558,333.526539566552));
#70961=CARTESIAN_POINT('Ctrl Pts',(17.6459195826621,2.2445516041575,328.789326567315));
#70962=CARTESIAN_POINT('Ctrl Pts',(17.3676815483882,-4.00803212309852,329.751556907862));
#70963=CARTESIAN_POINT('Ctrl Pts',(17.0894435141142,-6.58250392944424,335.530206007173));
#70964=CARTESIAN_POINT('Ctrl Pts',(16.8112054798403,-3.11630903733763,340.822292879527));
#70965=CARTESIAN_POINT('Ctrl Pts',(16.5329674455664,3.20967666168759,340.771347513243));
#70966=CARTESIAN_POINT('Ctrl Pts',(16.2547294112924,6.59018946303222,335.424121719004));
#70967=CARTESIAN_POINT('Ctrl Pts',(15.9764913770185,3.92298266518878,329.687685683262));
#70968=CARTESIAN_POINT('Ctrl Pts',(15.6982533427445,-2.34428742136838,328.82628208636));
#70969=CARTESIAN_POINT('Ctrl Pts',(15.4200153084707,-6.46023954296288,333.630408294877));
#70970=CARTESIAN_POINT('Ctrl Pts',(15.1417772741966,-4.6477251889569,339.691388596047));
#70971=CARTESIAN_POINT('Ctrl Pts',(14.8635392399228,1.42993797063821,341.447150827403));
#70972=CARTESIAN_POINT('Ctrl Pts',(14.5853012056488,6.19536816043845,337.286457904246));
#70973=CARTESIAN_POINT('Ctrl Pts',(14.3070631713749,5.27540043286967,331.027516310419));
#70974=CARTESIAN_POINT('Ctrl Pts',(14.0288251371009,-0.485724407125341,
328.414064364768));
#70975=CARTESIAN_POINT('Ctrl Pts',(13.750587102827,-5.80110712804899,331.844428343299));
#70976=CARTESIAN_POINT('Ctrl Pts',(13.472349068553,-5.7928994616363,338.170613855061));
#70977=CARTESIAN_POINT('Ctrl Pts',(13.1941110342791,-0.468633462574989,
341.587173830145));
#70978=CARTESIAN_POINT('Ctrl Pts',(12.9158730000052,5.28569054852431,338.958781607969));
#70979=CARTESIAN_POINT('Ctrl Pts',(12.6376349657312,6.18941435905494,332.697473935422));
#70980=CARTESIAN_POINT('Ctrl Pts',(12.3593969314573,1.4132039694968,328.549160447597));
#70981=CARTESIAN_POINT('Ctrl Pts',(12.0811588971833,-4.65988284705173,330.320687201855));
#70982=CARTESIAN_POINT('Ctrl Pts',(11.8029208629094,-6.45666394887963,336.386350246169));
#70983=CARTESIAN_POINT('Ctrl Pts',(11.5246828286355,-2.3282598558614,341.17978012878));
#70984=CARTESIAN_POINT('Ctrl Pts',(11.2464447943615,3.93675396228422,340.302117006826));
#70985=CARTESIAN_POINT('Ctrl Pts',(10.9682067600876,6.58906673699744,334.558779355101));
#70986=CARTESIAN_POINT('Ctrl Pts',(10.6899687258136,3.194690294589,329.220343398933));
#70987=CARTESIAN_POINT('Ctrl Pts',(10.4117306915397,-3.13140641536669,329.185812956169));
#70988=CARTESIAN_POINT('Ctrl Pts',(10.1334926572658,-6.58385741731503,334.486876225204));
#70989=CARTESIAN_POINT('Ctrl Pts',(9.8552546229919,-3.99440013610684,340.258825459627));
#70990=CARTESIAN_POINT('Ctrl Pts',(9.57701658871792,2.2606601201243,341.204828471322));
#70991=CARTESIAN_POINT('Ctrl Pts',(9.29877855444402,6.44114420034843,336.456751446593));
#70992=CARTESIAN_POINT('Ctrl Pts',(9.02054052017004,4.71068862539824,330.371836124353));
#70993=CARTESIAN_POINT('Ctrl Pts',(8.74230248589616,-1.34270261449642,328.534116584563));
#70994=CARTESIAN_POINT('Ctrl Pts',(8.46406445162217,-6.16390369514632,332.630046396311));
#70995=CARTESIAN_POINT('Ctrl Pts',(8.18582641734826,-5.32860359231034,338.900840894707));
#70996=CARTESIAN_POINT('Ctrl Pts',(7.9075883830743,0.396719405668529,341.591904035162));
#70997=CARTESIAN_POINT('Ctrl Pts',(7.62935034880038,5.75789950218825,338.233650055209));
#70998=CARTESIAN_POINT('Ctrl Pts',(7.35111231452643,5.83529005701858,331.907968623078));
#70999=CARTESIAN_POINT('Ctrl Pts',(7.07287428025249,0.55743811637587,328.419712881418));
#71000=CARTESIAN_POINT('Ctrl Pts',(6.79463624597856,-5.2314323012991,330.970251635584));
#71001=CARTESIAN_POINT('Ctrl Pts',(6.51639821170462,-6.22050336214957,337.218524847874));
#71002=CARTESIAN_POINT('Ctrl Pts',(6.23816017743065,-1.49920482391282,341.431468591223));
#71003=CARTESIAN_POINT('Ctrl Pts',(5.95992214315676,4.59428931436643,339.741257165524));
#71004=CARTESIAN_POINT('Ctrl Pts',(5.68168410888278,6.47851196515078,333.702124066768));
#71005=CARTESIAN_POINT('Ctrl Pts',(5.40344607460889,2.40427635277464,328.850148725226));
#71006=CARTESIAN_POINT('Ctrl Pts',(5.17158104604725,-2.80664825497015,329.515899410373));
#71007=CARTESIAN_POINT('Ctrl Pts',(4.98608902319796,-5.24601881533458,332.499051932022));
#71008=CARTESIAN_POINT('Ctrl Pts',(4.89334301177332,-5.62621912735357,334.369308258557));
#71009=CARTESIAN_POINT('Ctrl Pts',(4.846970006061,-5.57663578288216,335.297802782702));
#71010=CARTESIAN_POINT('Ctrl Pts',(185.229648962969,-2.58535847492491,329.674069654478));
#71011=CARTESIAN_POINT('Ctrl Pts',(185.183274228959,-3.47214497774874,330.104540455452));
#71012=CARTESIAN_POINT('Ctrl Pts',(185.090526489235,-5.01199270296094,331.416981243083));
#71013=CARTESIAN_POINT('Ctrl Pts',(184.905032738087,-6.52748388791409,335.210688764241));
#71014=CARTESIAN_POINT('Ctrl Pts',(184.673167709526,-4.47101474106914,340.386142168329));
#71015=CARTESIAN_POINT('Ctrl Pts',(184.394929675251,2.12056568075629,341.675688707916));
#71016=CARTESIAN_POINT('Ctrl Pts',(184.116691640978,6.75574576068523,336.828780790692));
#71017=CARTESIAN_POINT('Ctrl Pts',(183.838453606705,5.19669865427865,330.308915602165));
#71018=CARTESIAN_POINT('Ctrl Pts',(183.560215572429,-1.13414317430391,328.091207546338));
#71019=CARTESIAN_POINT('Ctrl Pts',(183.281977538157,-6.42268452913922,332.215067306152));
#71020=CARTESIAN_POINT('Ctrl Pts',(183.003739503882,-5.81802477444936,338.89383994989));
#71021=CARTESIAN_POINT('Ctrl Pts',(182.725501469609,0.126174998855868,341.999705536135));
#71022=CARTESIAN_POINT('Ctrl Pts',(182.447263435334,5.95436099319128,338.681826267342));
#71023=CARTESIAN_POINT('Ctrl Pts',(182.169025401061,6.31843686875824,331.985305041678));
#71024=CARTESIAN_POINT('Ctrl Pts',(181.890787366786,0.884113425449771,328.05526362586));
#71025=CARTESIAN_POINT('Ctrl Pts',(181.612549332511,-5.3615144597533,330.49833671817));
#71026=CARTESIAN_POINT('Ctrl Pts',(181.334311298238,-6.68697734938525,337.072502578512));
#71027=CARTESIAN_POINT('Ctrl Pts',(181.056073263964,-1.87589045730543,341.744772511905));
#71028=CARTESIAN_POINT('Ctrl Pts',(180.77783522969,4.6566684581192,340.227459444797));
#71029=CARTESIAN_POINT('Ctrl Pts',(180.499597195416,6.91587408932694,333.912986554537));
#71030=CARTESIAN_POINT('Ctrl Pts',(180.221359161143,2.82848275536695,328.59604850725));
#71031=CARTESIAN_POINT('Ctrl Pts',(179.943121126868,-3.85456471789821,329.155922938523));
#71032=CARTESIAN_POINT('Ctrl Pts',(179.664883092594,-7.00033543312608,335.078820251569));
#71033=CARTESIAN_POINT('Ctrl Pts',(179.38664505832,-3.72200143945353,340.929385583913));
#71034=CARTESIAN_POINT('Ctrl Pts',(179.108407024047,2.97195822908398,341.338641177155));
#71035=CARTESIAN_POINT('Ctrl Pts',(178.830168989773,6.93859575479861,335.931019376625));
#71036=CARTESIAN_POINT('Ctrl Pts',(178.5519309555,4.53778633913574,329.669014806167));
#71037=CARTESIAN_POINT('Ctrl Pts',(178.273692921225,-2.02728260607429,328.29917667867));
#71038=CARTESIAN_POINT('Ctrl Pts',(177.995454886951,-6.73194423494412,333.078585200804));
#71039=CARTESIAN_POINT('Ctrl Pts',(177.717216852677,-5.25879999817888,339.621247728553));
#71040=CARTESIAN_POINT('Ctrl Pts',(177.438978818404,1.04026737473892,341.923059422968));
#71041=CARTESIAN_POINT('Ctrl Pts',(177.16074078413,6.38469673345932,337.871681670357));
#71042=CARTESIAN_POINT('Ctrl Pts',(176.882502749856,5.86998413717594,331.185004034154));
#71043=CARTESIAN_POINT('Ctrl Pts',(176.604264715582,-0.0315262606111309,
327.999291886908));
#71044=CARTESIAN_POINT('Ctrl Pts',(176.326026681307,-5.90410547455225,331.238026244579));
#71045=CARTESIAN_POINT('Ctrl Pts',(176.047788647034,-6.35857423885009,337.929068391057));
#71046=CARTESIAN_POINT('Ctrl Pts',(175.76955061276,-0.977873276610438,341.932147707987));
#71047=CARTESIAN_POINT('Ctrl Pts',(175.491312578485,5.30020755821694,339.573697391659));
#71048=CARTESIAN_POINT('Ctrl Pts',(175.213074544211,6.714366147789,333.018032486652));
#71049=CARTESIAN_POINT('Ctrl Pts',(174.934836509937,1.96685002742494,328.281189914862));
#71050=CARTESIAN_POINT('Ctrl Pts',(174.656598475665,-4.58561533245236,329.710100188722));
#71051=CARTESIAN_POINT('Ctrl Pts',(174.37836044139,-6.92992918530729,335.993473440603));
#71052=CARTESIAN_POINT('Ctrl Pts',(174.100122407116,-2.914749310394,341.365150779684));
#71053=CARTESIAN_POINT('Ctrl Pts',(173.821884372842,3.77525298503917,340.895623197721));
#71054=CARTESIAN_POINT('Ctrl Pts',(173.543646338568,7.0007613387443,335.015769226465));
#71055=CARTESIAN_POINT('Ctrl Pts',(173.265408304295,3.80177434295197,329.121444068835));
#71056=CARTESIAN_POINT('Ctrl Pts',(172.98717027002,-2.88604485327017,328.621782921892));
#71057=CARTESIAN_POINT('Ctrl Pts',(172.708932235747,-6.92538328559842,333.975317445198));
#71058=CARTESIAN_POINT('Ctrl Pts',(172.430694201473,-4.60939969522278,340.269188024757));
#71059=CARTESIAN_POINT('Ctrl Pts',(172.152456167198,1.93656196083081,341.727602527083));
#71060=CARTESIAN_POINT('Ctrl Pts',(171.874218132924,6.70536928903767,337.012195489557));
#71061=CARTESIAN_POINT('Ctrl Pts',(171.59598009865,5.32075819178314,330.450226351219));
#71062=CARTESIAN_POINT('Ctrl Pts',(171.317742064377,-0.946634163808588,
328.06351733582));
#71063=CARTESIAN_POINT('Ctrl Pts',(171.039504030103,-6.34531431957053,332.042316079022));
#71064=CARTESIAN_POINT('Ctrl Pts',(170.76126599583,-5.92099318094844,338.735337701162));
#71065=CARTESIAN_POINT('Ctrl Pts',(170.483027961555,-0.0630639938860975,
342.000495048441));
#71066=CARTESIAN_POINT('Ctrl Pts',(170.204789927282,5.85273808954251,338.841401416901));
#71067=CARTESIAN_POINT('Ctrl Pts',(169.926551893006,6.39756881447056,332.157110404065));
#71068=CARTESIAN_POINT('Ctrl Pts',(169.648313858733,1.07144506631992,328.081697212435));
#71069=CARTESIAN_POINT('Ctrl Pts',(169.370075824459,-5.23792800468925,330.355108374972));
#71070=CARTESIAN_POINT('Ctrl Pts',(169.091837790186,-6.74053185748574,336.891068023309));
#71071=CARTESIAN_POINT('Ctrl Pts',(168.813599755911,-2.05744911475468,341.691622458773));
#71072=CARTESIAN_POINT('Ctrl Pts',(168.535361721638,4.51372431268757,340.351373732007));
#71073=CARTESIAN_POINT('Ctrl Pts',(168.257123687364,6.9427195608381,334.100248317525));
#71074=CARTESIAN_POINT('Ctrl Pts',(167.978885653089,3.00048354238029,328.674811741737));
#71075=CARTESIAN_POINT('Ctrl Pts',(167.700647618815,-3.69525193585539,329.053907070932));
#71076=CARTESIAN_POINT('Ctrl Pts',(167.422409584541,-6.99990925438579,334.889644116945));
#71077=CARTESIAN_POINT('Ctrl Pts',(167.144171550268,-3.88085316865759,340.826653127987));
#71078=CARTESIAN_POINT('Ctrl Pts',(166.865933515994,2.79960458864882,341.416628564735));
#71079=CARTESIAN_POINT('Ctrl Pts',(166.587695481719,6.91090653704819,336.118158676908));
#71080=CARTESIAN_POINT('Ctrl Pts',(166.309457447446,4.68017156121173,329.793571075277));
#71081=CARTESIAN_POINT('Ctrl Pts',(166.031219413172,-1.84548777712974,328.2468464511));
#71082=CARTESIAN_POINT('Ctrl Pts',(165.752981378897,-6.67757022175417,332.897391162365));
#71083=CARTESIAN_POINT('Ctrl Pts',(165.474743344624,-5.38174503464973,339.477468969471));
#71084=CARTESIAN_POINT('Ctrl Pts',(165.196505310349,0.852828136326283,341.948639590629));
#71085=CARTESIAN_POINT('Ctrl Pts',(164.918267276077,6.30477351431828,338.043146221218));
#71086=CARTESIAN_POINT('Ctrl Pts',(164.640029241802,5.97092129652498,331.345002481359));
#71087=CARTESIAN_POINT('Ctrl Pts',(164.361791207529,0.157642735564626,328.000996016683));
#71088=CARTESIAN_POINT('Ctrl Pts',(164.083553173255,-5.80030223702046,331.079872202367));
#71089=CARTESIAN_POINT('Ctrl Pts',(163.80531513898,-6.43539545901254,337.756191806947));
#71090=CARTESIAN_POINT('Ctrl Pts',(163.527077104706,-1.1648212545501,341.903194871616));
#71091=CARTESIAN_POINT('Ctrl Pts',(163.248839070432,5.17469222247944,339.715237893593));
#71092=CARTESIAN_POINT('Ctrl Pts',(162.970601036159,6.76546702527161,333.200176697417));
#71093=CARTESIAN_POINT('Ctrl Pts',(162.692363001885,2.14767259710162,328.336786780673));
#71094=CARTESIAN_POINT('Ctrl Pts',(162.414124967611,-4.44100927383294,329.588129286439));
#71095=CARTESIAN_POINT('Ctrl Pts',(162.135886933336,-6.95424248336044,335.805865666961));
#71096=CARTESIAN_POINT('Ctrl Pts',(161.857648899064,-3.08567001035892,341.284071019469));
#71097=CARTESIAN_POINT('Ctrl Pts',(161.579410864788,3.61457628673427,340.995477150148));
#71098=CARTESIAN_POINT('Ctrl Pts',(161.301172830515,6.99777927655,335.204922393233));
#71099=CARTESIAN_POINT('Ctrl Pts',(161.022934796242,3.9592235113286,329.226313380698));
#71100=CARTESIAN_POINT('Ctrl Pts',(160.744696761967,-2.71265323219581,328.546131359222));
#71101=CARTESIAN_POINT('Ctrl Pts',(160.466458727693,-6.89516814323021,333.788569330442));
#71102=CARTESIAN_POINT('Ctrl Pts',(160.188220693419,-4.75008902173721,340.142719346428));
#71103=CARTESIAN_POINT('Ctrl Pts',(159.909982659145,1.75407668380499,341.77747172461));
#71104=CARTESIAN_POINT('Ctrl Pts',(159.631744624871,6.64855210674876,337.192638336435));
#71105=CARTESIAN_POINT('Ctrl Pts',(159.353506590598,5.44174939379744,330.595653110203));
#71106=CARTESIAN_POINT('Ctrl Pts',(159.075268556323,-0.758866417752336,
328.040472016683));
#71107=CARTESIAN_POINT('Ctrl Pts',(158.79703052205,-6.26308171858079,331.871947030989));
#71108=CARTESIAN_POINT('Ctrl Pts',(158.518792487775,-6.01975936920231,338.573990084969));
#71109=CARTESIAN_POINT('Ctrl Pts',(158.240554453501,-0.252192698209519,
341.996235189982));
#71110=CARTESIAN_POINT('Ctrl Pts',(157.962316419228,5.74680748957203,338.998138525409));
#71111=CARTESIAN_POINT('Ctrl Pts',(157.684078384953,6.47204726691282,332.331009148498));
#71112=CARTESIAN_POINT('Ctrl Pts',(157.405840350679,1.2579847946688,328.113173281769));
#71113=CARTESIAN_POINT('Ctrl Pts',(157.127602316405,-5.11051175581766,330.215276644966));
#71114=CARTESIAN_POINT('Ctrl Pts',(156.849364282132,-6.78916709902012,336.708250008677));
#71115=CARTESIAN_POINT('Ctrl Pts',(156.571126247859,-2.23750400339395,341.633587553154));
#71116=CARTESIAN_POINT('Ctrl Pts',(156.292888213583,4.36748349064183,340.471379711693));
#71117=CARTESIAN_POINT('Ctrl Pts',(156.014650179311,6.96449584926633,334.288167466244));
#71118=CARTESIAN_POINT('Ctrl Pts',(155.736412145036,3.17029316280935,328.758193430391));
#71119=CARTESIAN_POINT('Ctrl Pts',(155.458174110763,-3.53324076570739,328.956233154555));
#71120=CARTESIAN_POINT('Ctrl Pts',(155.179936076489,-6.99437179408267,334.70054850693));
#71121=CARTESIAN_POINT('Ctrl Pts',(154.901698042215,-4.03687106378675,340.719666074599));
#71122=CARTESIAN_POINT('Ctrl Pts',(154.623460007941,2.62520665762704,341.489930507742));
#71123=CARTESIAN_POINT('Ctrl Pts',(154.345221973666,6.87817097732325,336.304481505147));
#71124=CARTESIAN_POINT('Ctrl Pts',(154.066983939393,4.81913931276712,329.921929079394));
#71125=CARTESIAN_POINT('Ctrl Pts',(153.788745905119,-1.6623453687357,328.199447385277));
#71126=CARTESIAN_POINT('Ctrl Pts',(153.510507870844,-6.61832024152719,332.7177324497));
#71127=CARTESIAN_POINT('Ctrl Pts',(153.23226983657,-5.50076031491589,339.330420758819));
#71128=CARTESIAN_POINT('Ctrl Pts',(152.954031802296,0.664766161604575,341.969145854475));
#71129=CARTESIAN_POINT('Ctrl Pts',(152.675793768022,6.22024654355298,338.212388663904));
#71130=CARTESIAN_POINT('Ctrl Pts',(152.397555733748,6.0674984831713,331.507669811247));
#71131=CARTESIAN_POINT('Ctrl Pts',(152.119317699474,0.346696620914136,328.0078108261));
#71132=CARTESIAN_POINT('Ctrl Pts',(151.841079665202,-5.6922636131222,330.924580641298));
#71133=CARTESIAN_POINT('Ctrl Pts',(151.562841630926,-6.50751754706949,337.581302648885));
#71134=CARTESIAN_POINT('Ctrl Pts',(151.284603596654,-1.35091867887267,341.869201315556));
#71135=CARTESIAN_POINT('Ctrl Pts',(151.00636556238,5.04539832139854,339.853335324186));
#71136=CARTESIAN_POINT('Ctrl Pts',(150.728127528106,6.81162775207952,333.383635140922));
#71137=CARTESIAN_POINT('Ctrl Pts',(150.449889493832,2.32692693413808,328.397249131329));
#71138=CARTESIAN_POINT('Ctrl Pts',(150.171651459557,-4.29316038587669,329.470110137471));
#71139=CARTESIAN_POINT('Ctrl Pts',(149.893413425284,-6.97347778671582,335.617669449416));
#71140=CARTESIAN_POINT('Ctrl Pts',(149.61517539101,-3.25433755104927,341.198402624417));
#71141=CARTESIAN_POINT('Ctrl Pts',(149.336937356736,3.45126022127169,341.090953199264));
#71142=CARTESIAN_POINT('Ctrl Pts',(149.058699322462,6.98968742904898,335.393925925467));
#71143=CARTESIAN_POINT('Ctrl Pts',(148.780461288187,4.11378165080535,329.335398644207));
#71144=CARTESIAN_POINT('Ctrl Pts',(148.502223253914,-2.5372808290647,328.475192417778));
#71145=CARTESIAN_POINT('Ctrl Pts',(148.22398521964,-6.85991814230574,333.602705803552));
#71146=CARTESIAN_POINT('Ctrl Pts',(147.945747185366,-4.88730982857861,340.012495449378));
#71147=CARTESIAN_POINT('Ctrl Pts',(147.667509151092,1.57031057826028,341.822392005622));
#71148=CARTESIAN_POINT('Ctrl Pts',(147.389271116818,6.58688014517586,337.371480116646));
#71149=CARTESIAN_POINT('Ctrl Pts',(147.111033082543,5.55876702505512,330.744295927614));
#71150=CARTESIAN_POINT('Ctrl Pts',(146.83279504827,-0.570544546691902,328.022508551721));
#71151=CARTESIAN_POINT('Ctrl Pts',(146.554557013996,-6.17627580916347,331.703862090309));
#71152=CARTESIAN_POINT('Ctrl Pts',(146.276318979723,-6.11412992324723,338.410032737704));
#71153=CARTESIAN_POINT('Ctrl Pts',(145.998080945448,-0.44113725117675,341.986866673709));
#71154=CARTESIAN_POINT('Ctrl Pts',(145.719842911175,5.63668056512349,339.151956189233));
#71155=CARTESIAN_POINT('Ctrl Pts',(145.4416048769,6.54179982407865,332.506856792673));
#71156=CARTESIAN_POINT('Ctrl Pts',(145.163366842627,1.44360594128398,328.149678118741));
#71157=CARTESIAN_POINT('Ctrl Pts',(144.885128808353,-4.97936380623825,330.078938724656));
#71158=CARTESIAN_POINT('Ctrl Pts',(144.606890774078,-6.83284488406494,336.524184628209));
#71159=CARTESIAN_POINT('Ctrl Pts',(144.328652739805,-2.41592506441045,341.570708795382));
#71160=CARTESIAN_POINT('Ctrl Pts',(144.05041470553,4.21805352785792,340.587390484536));
#71161=CARTESIAN_POINT('Ctrl Pts',(143.772176671257,6.98118665597922,334.47660639578));
#71162=CARTESIAN_POINT('Ctrl Pts',(143.493938636982,3.33778783205454,328.846132892339));
#71163=CARTESIAN_POINT('Ctrl Pts',(143.215700602708,-3.36864961967894,328.86297240267));
#71164=CARTESIAN_POINT('Ctrl Pts',(142.937462568435,-6.98372703661993,334.511671556691));
#71165=CARTESIAN_POINT('Ctrl Pts',(142.659224534161,-4.18994123169692,340.608502515421));
#71166=CARTESIAN_POINT('Ctrl Pts',(142.380986499886,2.44889179812317,341.558493497111));
#71167=CARTESIAN_POINT('Ctrl Pts',(142.102748465614,6.8404129703893,336.489851799707));
#71168=CARTESIAN_POINT('Ctrl Pts',(141.82451043134,4.95458812405912,330.053995095889));
#71169=CARTESIAN_POINT('Ctrl Pts',(141.546272397066,-1.47798911411928,328.15701408966));
#71170=CARTESIAN_POINT('Ctrl Pts',(141.268034362791,-6.55423755735398,332.539740251045));
#71171=CARTESIAN_POINT('Ctrl Pts',(140.989796328518,-5.61575893459271,339.18021047067));
#71172=CARTESIAN_POINT('Ctrl Pts',(140.711558294244,0.476218773978294,341.984563241168));
#71173=CARTESIAN_POINT('Ctrl Pts',(140.433320259969,6.13117754264699,338.37928541723));
#71174=CARTESIAN_POINT('Ctrl Pts',(140.155082225696,6.15964517646074,331.672887244071));
#71175=CARTESIAN_POINT('Ctrl Pts',(139.876844191421,0.535497348050235,328.019731338925));
#71176=CARTESIAN_POINT('Ctrl Pts',(139.598606157147,-5.58006849273806,330.772264955451));
#71177=CARTESIAN_POINT('Ctrl Pts',(139.320368122873,-6.5748878394166,337.404528621092));
#71178=CARTESIAN_POINT('Ctrl Pts',(139.042130088599,-1.53602966104794,341.830191861942));
#71179=CARTESIAN_POINT('Ctrl Pts',(138.763892054326,4.9124202655037,339.987888844554));
#71180=CARTESIAN_POINT('Ctrl Pts',(138.485654020052,6.85281462160694,333.568273855638));
#71181=CARTESIAN_POINT('Ctrl Pts',(138.207415985779,2.50448214683961,328.462532817158));
#71182=CARTESIAN_POINT('Ctrl Pts',(137.929177951504,-4.14217662798657,329.356128919516));
#71183=CARTESIAN_POINT('Ctrl Pts',(137.650939917231,-6.98762104973629,335.429022209032));
#71184=CARTESIAN_POINT('Ctrl Pts',(137.372701882957,-3.42062877126065,341.108208149678));
#71185=CARTESIAN_POINT('Ctrl Pts',(137.094463848682,3.28542404220298,341.181981628368));
#71186=CARTESIAN_POINT('Ctrl Pts',(136.816225814409,6.97649170491632,335.582641812605));
#71187=CARTESIAN_POINT('Ctrl Pts',(136.537987780135,4.26533590287672,329.448620205192));
#71188=CARTESIAN_POINT('Ctrl Pts',(136.259749745861,-2.3600557009781,328.409017897245));
#71189=CARTESIAN_POINT('Ctrl Pts',(135.981511711587,-6.81965902241038,333.417862582258));
#71190=CARTESIAN_POINT('Ctrl Pts',(135.703273677312,-5.0209619169788,339.878611423224));
#71191=CARTESIAN_POINT('Ctrl Pts',(135.425035643039,1.38539783038779,341.862330569284));
#71192=CARTESIAN_POINT('Ctrl Pts',(135.146797608765,6.52039843724598,337.548590239744));
#71193=CARTESIAN_POINT('Ctrl Pts',(134.868559574491,5.6717256391667,330.896046264323));
#71194=CARTESIAN_POINT('Ctrl Pts',(134.590321540217,-0.381806063442646,
328.009640057873));
#71195=CARTESIAN_POINT('Ctrl Pts',(134.312083505942,-6.08495997707894,331.538183992771));
#71196=CARTESIAN_POINT('Ctrl Pts',(134.033845471669,-6.20403593361193,338.243585381181));
#71197=CARTESIAN_POINT('Ctrl Pts',(133.755607437395,-0.62975968528953,341.972396340524));
#71198=CARTESIAN_POINT('Ctrl Pts',(133.477369403122,5.52243773098536,339.302742090568));
#71199=CARTESIAN_POINT('Ctrl Pts',(133.199131368848,6.60677555258225,332.684524932468));
#71200=CARTESIAN_POINT('Ctrl Pts',(132.920893334573,1.62817296542187,328.191185067485));
#71201=CARTESIAN_POINT('Ctrl Pts',(132.6426553003,-4.8445799203126,329.946194168128));
#71202=CARTESIAN_POINT('Ctrl Pts',(132.364417266025,-6.87153331905868,336.339006286627));
#71203=CARTESIAN_POINT('Ctrl Pts',(132.086179231752,-2.59258201457014,341.503032099589));
#71204=CARTESIAN_POINT('Ctrl Pts',(131.807941197478,4.0655435382416,340.699321339354));
#71205=CARTESIAN_POINT('Ctrl Pts',(131.529703163203,6.99277979333328,334.66542750784));
#71206=CARTESIAN_POINT('Ctrl Pts',(131.25146512893,3.50284524534358,328.938565914098));
#71207=CARTESIAN_POINT('Ctrl Pts',(130.973227094655,-3.20159868238686,328.774192914369));
#71208=CARTESIAN_POINT('Ctrl Pts',(130.694989060382,-6.96798275480997,334.32315118436));
#71209=CARTESIAN_POINT('Ctrl Pts',(130.416751026107,-4.33995190040084,340.493243622194));
#71210=CARTESIAN_POINT('Ctrl Pts',(130.138512991833,2.27078875542109,341.622267468082));
#71211=CARTESIAN_POINT('Ctrl Pts',(129.86027495756,6.79766008718017,336.674134203019));
#71212=CARTESIAN_POINT('Ctrl Pts',(129.582036923286,5.08641909023244,330.189672690026));
#71213=CARTESIAN_POINT('Ctrl Pts',(129.303798889013,-1.2925536303989,328.119577549082));
#71214=CARTESIAN_POINT('Ctrl Pts',(129.025560854738,-6.48536896247348,332.363544536476));
#71215=CARTESIAN_POINT('Ctrl Pts',(128.747322820465,-5.72665692157511,339.026947788727));
#71216=CARTESIAN_POINT('Ctrl Pts',(128.469084786191,0.287323650935115,341.994880492916));
#71217=CARTESIAN_POINT('Ctrl Pts',(128.190846751916,6.03763154987234,338.543714613022));
#71218=CARTESIAN_POINT('Ctrl Pts',(127.912608717642,6.24729409078729,331.840534137901));
#71219=CARTESIAN_POINT('Ctrl Pts',(127.634370683369,0.723907054496541,328.036748850787));
#71220=CARTESIAN_POINT('Ctrl Pts',(127.356132649094,-5.46379880085513,330.623036365888));
#71221=CARTESIAN_POINT('Ctrl Pts',(127.077894614821,-6.63745714220019,337.225998804136));
#71222=CARTESIAN_POINT('Ctrl Pts',(126.799656580547,-1.72001903285498,341.786194995516));
#71223=CARTESIAN_POINT('Ctrl Pts',(126.521418546272,4.77585515550195,340.118800203585));
#71224=CARTESIAN_POINT('Ctrl Pts',(126.243180511998,6.88899755916128,333.753958018191));
#71225=CARTESIAN_POINT('Ctrl Pts',(125.964942477725,2.6802085842156,328.532590167953));
#71226=CARTESIAN_POINT('Ctrl Pts',(125.68670444345,-3.98816824865087,329.246268861772));
#71227=CARTESIAN_POINT('Ctrl Pts',(125.408466409176,-6.99666194499731,335.24006169621));
#71228=CARTESIAN_POINT('Ctrl Pts',(125.130228374903,-3.58442224498074,341.013553455341));
#71229=CARTESIAN_POINT('Ctrl Pts',(124.851990340629,3.11718884326904,341.268495968409));
#71230=CARTESIAN_POINT('Ctrl Pts',(124.573752306356,6.95820173968273,335.770932254116));
#71231=CARTESIAN_POINT('Ctrl Pts',(124.29551427208,4.4137756024789,329.565895389163));
#71232=CARTESIAN_POINT('Ctrl Pts',(124.017276237808,-2.18110725789871,328.347656118321));
#71233=CARTESIAN_POINT('Ctrl Pts',(123.739038203534,-6.77442018079302,333.234174639263));
#71234=CARTESIAN_POINT('Ctrl Pts',(123.460800169259,-5.15094769405156,339.741165030212));
#71235=CARTESIAN_POINT('Ctrl Pts',(123.182562134986,1.19947346365769,341.897258252417));
#71236=CARTESIAN_POINT('Ctrl Pts',(122.904324100712,6.44915552796757,337.723839379744));
#71237=CARTESIAN_POINT('Ctrl Pts',(122.626086066438,5.78054275364118,331.050793312083));
#71238=CARTESIAN_POINT('Ctrl Pts',(122.347848032164,-0.192788785030493,
328.001875931728));
#71239=CARTESIAN_POINT('Ctrl Pts',(122.06960999789,-5.98920090123743,331.375033716685));
#71240=CARTESIAN_POINT('Ctrl Pts',(121.791371963616,-6.28941175083933,338.074769555423));
#71241=CARTESIAN_POINT('Ctrl Pts',(121.513133929341,-0.817922268261233,
341.952834756677));
#71242=CARTESIAN_POINT('Ctrl Pts',(121.234895895067,5.40416240738729,339.450386125398));
#71243=CARTESIAN_POINT('Ctrl Pts',(120.956657860793,6.66692700708289,332.863883834436));
#71244=CARTESIAN_POINT('Ctrl Pts',(120.67841982652,1.81155109605984,328.237663819586));
#71245=CARTESIAN_POINT('Ctrl Pts',(120.400181792245,-4.70625851736698,329.817139905586));
#71246=CARTESIAN_POINT('Ctrl Pts',(120.121943757973,-6.90520415366798,336.152850201338));
#71247=CARTESIAN_POINT('Ctrl Pts',(119.843705723699,-2.7673458587941,341.430606883365));
#71248=CARTESIAN_POINT('Ctrl Pts',(119.565467689425,3.91006488473719,340.807090544128));
#71249=CARTESIAN_POINT('Ctrl Pts',(119.287229655151,6.99926679600826,334.854492925062));
#71250=CARTESIAN_POINT('Ctrl Pts',(119.008991620877,3.66534487759111,329.035425000985));
#71251=CARTESIAN_POINT('Ctrl Pts',(118.730753586603,-3.03220993458969,328.689959516521));
#71252=CARTESIAN_POINT('Ctrl Pts',(118.452515552329,-6.9471504451428,334.135125047702));
#71253=CARTESIAN_POINT('Ctrl Pts',(118.174277518055,-4.48679353196085,340.373973557072));
#71254=CARTESIAN_POINT('Ctrl Pts',(117.896039483781,2.09102758053759,341.681205852838));
#71255=CARTESIAN_POINT('Ctrl Pts',(117.617801449507,6.74994354589319,336.85719415189));
#71256=CARTESIAN_POINT('Ctrl Pts',(117.339563415233,5.21453594818604,330.328862789894));
#71257=CARTESIAN_POINT('Ctrl Pts',(117.061325380959,-1.10617432274702,328.08716509974));
#71258=CARTESIAN_POINT('Ctrl Pts',(116.783087346685,-6.41176474480132,332.189273964279));
#71259=CARTESIAN_POINT('Ctrl Pts',(116.50484931241,-5.83337329804406,338.87074462555));
#71260=CARTESIAN_POINT('Ctrl Pts',(116.226611278137,0.0982187238792476,
342.000090076052));
#71261=CARTESIAN_POINT('Ctrl Pts',(115.948373243863,5.93967687260467,338.705556184921));
#71262=CARTESIAN_POINT('Ctrl Pts',(115.67013520959,6.33038122482778,332.010488076808));
#71263=CARTESIAN_POINT('Ctrl Pts',(115.391897175315,0.911788163300145,328.058850935484));
#71264=CARTESIAN_POINT('Ctrl Pts',(115.113659141041,-5.34353943771679,330.477003839475));
#71265=CARTESIAN_POINT('Ctrl Pts',(114.835421106768,-6.69517976725385,337.045843560665));
#71266=CARTESIAN_POINT('Ctrl Pts',(114.557183072494,-1.90275244507342,341.737242842834));
#71267=CARTESIAN_POINT('Ctrl Pts',(114.27894503822,4.63580271137082,340.245973809676));
#71268=CARTESIAN_POINT('Ctrl Pts',(114.000707003946,6.92015014392593,333.940552041823));
#71269=CARTESIAN_POINT('Ctrl Pts',(113.722468969672,2.8539779306489,328.607370027764));
#71270=CARTESIAN_POINT('Ctrl Pts',(113.444230935398,-3.83124770493942,329.140610184161));
#71271=CARTESIAN_POINT('Ctrl Pts',(113.165992901124,-7.00059387082826,335.050925890101));
#71272=CARTESIAN_POINT('Ctrl Pts',(112.88775486685,-3.74559837005416,340.914507658361));
#71273=CARTESIAN_POINT('Ctrl Pts',(112.609516832576,2.94667746997732,341.350433046532));
#71274=CARTESIAN_POINT('Ctrl Pts',(112.331278798301,6.93483088869879,335.95865976014));
#71275=CARTESIAN_POINT('Ctrl Pts',(112.053040764028,4.55899235879751,329.687138561661));
#71276=CARTESIAN_POINT('Ctrl Pts',(111.774802729754,-2.00056616815533,328.291151887441));
#71277=CARTESIAN_POINT('Ctrl Pts',(111.496564695481,-6.72423465090026,333.05177610368));
#71278=CARTESIAN_POINT('Ctrl Pts',(111.218326661206,-5.27717224405479,339.600256633835));
#71279=CARTESIAN_POINT('Ctrl Pts',(110.940088626933,1.01267324022512,341.927149550796));
#71280=CARTESIAN_POINT('Ctrl Pts',(110.661850592658,6.37320343898297,337.897099569552));
#71281=CARTESIAN_POINT('Ctrl Pts',(110.383612558385,5.88513891011469,331.208424074449));
#71282=CARTESIAN_POINT('Ctrl Pts',(110.105374524111,-0.00363073205790497,
327.999221842656));
#71283=CARTESIAN_POINT('Ctrl Pts',(109.827136489837,-5.88906850501048,331.214530394541));
#71284=CARTESIAN_POINT('Ctrl Pts',(109.548898455563,-6.37019503342358,337.903708529916));
#71285=CARTESIAN_POINT('Ctrl Pts',(109.270660421289,-1.00548760358844,341.928196206054));
#71286=CARTESIAN_POINT('Ctrl Pts',(108.992422387014,5.28194095908712,339.594780483906));
#71287=CARTESIAN_POINT('Ctrl Pts',(108.714184352741,6.72221026492919,333.044802530524));
#71288=CARTESIAN_POINT('Ctrl Pts',(108.435946318467,1.99360643030661,328.289080436214));
#71289=CARTESIAN_POINT('Ctrl Pts',(108.157708284192,-4.56450059982566,329.69187017258));
#71290=CARTESIAN_POINT('Ctrl Pts',(107.879470249919,-6.93383280141635,335.9658523037));
#71291=CARTESIAN_POINT('Ctrl Pts',(107.601232215645,-2.94008898435164,341.353486031673));
#71292=CARTESIAN_POINT('Ctrl Pts',(107.32299418137,3.75173109801029,340.910619405679));
#71293=CARTESIAN_POINT('Ctrl Pts',(107.044756147098,7.00064292718842,335.043664591693));
#71294=CARTESIAN_POINT('Ctrl Pts',(106.766518112823,3.82516807140595,329.1366394264));
#71295=CARTESIAN_POINT('Ctrl Pts',(106.48828007855,-2.86060706411756,328.610333716438));
#71296=CARTESIAN_POINT('Ctrl Pts',(106.210042044276,-6.92124531939146,333.947730443583));
#71297=CARTESIAN_POINT('Ctrl Pts',(105.931804010002,-4.63035890247325,340.250779411178));
#71298=CARTESIAN_POINT('Ctrl Pts',(105.653565975728,1.90973953525927,341.735265614511));
#71299=CARTESIAN_POINT('Ctrl Pts',(105.375327941454,6.69729818919371,337.038897975766));
#71300=CARTESIAN_POINT('Ctrl Pts',(105.09708990718,5.3388451468643,330.471463758743));
#71301=CARTESIAN_POINT('Ctrl Pts',(104.818851872906,-0.918987285517264,
328.059800409238));
#71302=CARTESIAN_POINT('Ctrl Pts',(104.540613838632,-6.33347865020975,332.017055786995));
#71303=CARTESIAN_POINT('Ctrl Pts',(104.262375804358,-5.93583013959639,338.711715040844));
#71304=CARTESIAN_POINT('Ctrl Pts',(103.984137770084,-0.0909579225846602,
342.000188186533));
#71305=CARTESIAN_POINT('Ctrl Pts',(103.70589973581,5.83738503744626,338.864691956051));
#71306=CARTESIAN_POINT('Ctrl Pts',(103.427661701535,6.40884590827468,332.182624960259));
#71307=CARTESIAN_POINT('Ctrl Pts',(103.149423667262,1.09900348349006,328.086021454053));
#71308=CARTESIAN_POINT('Ctrl Pts',(102.871185632988,-5.21937821682842,330.334274009303));
#71309=CARTESIAN_POINT('Ctrl Pts',(102.592947598715,-6.74801356545994,336.864194440215));
#71310=CARTESIAN_POINT('Ctrl Pts',(102.31470956444,-2.08409646558584,341.683371148806));
#71311=CARTESIAN_POINT('Ctrl Pts',(102.036471530166,4.49236519954295,340.369316800534));
#71312=CARTESIAN_POINT('Ctrl Pts',(101.758233495893,6.94624962825285,334.127919675399));
#71313=CARTESIAN_POINT('Ctrl Pts',(101.479995461619,3.02566329959154,328.686817792265));
#71314=CARTESIAN_POINT('Ctrl Pts',(101.201757427344,-3.67152958038781,329.039230038754));
#71315=CARTESIAN_POINT('Ctrl Pts',(100.923519393071,-6.99941395613305,334.861752897858));
#71316=CARTESIAN_POINT('Ctrl Pts',(100.645281358797,-3.90403945551564,340.811143082075));
#71317=CARTESIAN_POINT('Ctrl Pts',(100.367043324523,2.77401442990058,341.427733032202));
#71318=CARTESIAN_POINT('Ctrl Pts',(100.088805290249,6.90639621738289,336.145687251863));
#71319=CARTESIAN_POINT('Ctrl Pts',(99.8105672559745,4.70088013441401,329.812261190805));
#71320=CARTESIAN_POINT('Ctrl Pts',(99.5323292217006,-1.81856426302957,328.239546464046));
#71321=CARTESIAN_POINT('Ctrl Pts',(99.2540911874266,-6.66913907825543,332.870800163102));
#71322=CARTESIAN_POINT('Ctrl Pts',(98.9758531531527,-5.39954339769772,339.455989125541));
#71323=CARTESIAN_POINT('Ctrl Pts',(98.6976151188788,0.825133561797275,341.951982637763));
#71324=CARTESIAN_POINT('Ctrl Pts',(98.4193770846049,6.29259763058232,338.068244294405));
#71325=CARTESIAN_POINT('Ctrl Pts',(98.1411390503309,5.98543773237075,331.368823449284));
#71326=CARTESIAN_POINT('Ctrl Pts',(97.862901016057,0.185529972078658,328.001679728676));
#71327=CARTESIAN_POINT('Ctrl Pts',(97.5846629817831,-5.78463590517213,331.056791226025));
#71328=CARTESIAN_POINT('Ctrl Pts',(97.306424947509,-6.44632679333245,337.730527213584));
#71329=CARTESIAN_POINT('Ctrl Pts',(97.0281869132352,-1.19231873087909,341.898498679754));
#71330=CARTESIAN_POINT('Ctrl Pts',(96.7499488789612,5.15586263230639,339.735819729186));
#71331=CARTESIAN_POINT('Ctrl Pts',(96.4717108446873,6.772584958232,333.22714891373));
#71332=CARTESIAN_POINT('Ctrl Pts',(96.1934728104133,2.17420603117824,328.345397372904));
#71333=CARTESIAN_POINT('Ctrl Pts',(95.9152347761393,-4.4194096794594,329.570476441191));
#71334=CARTESIAN_POINT('Ctrl Pts',(95.6369967418656,-6.95739835763707,335.77814913976));
#71335=CARTESIAN_POINT('Ctrl Pts',(95.3587587075914,-3.11068525404265,341.271725858234));
#71336=CARTESIAN_POINT('Ctrl Pts',(95.0805206733176,3.59065779354763,341.009832327129));
#71337=CARTESIAN_POINT('Ctrl Pts',(94.8022826390436,6.9969071820214,335.232804374397));
#71338=CARTESIAN_POINT('Ctrl Pts',(94.5240446047697,3.98219812373486,329.242135283468));
#71339=CARTESIAN_POINT('Ctrl Pts',(94.2458065704957,-2.68691537555521,328.535373656956));
#71340=CARTESIAN_POINT('Ctrl Pts',(93.9675685362218,-6.8902862935042,333.761104207728));
#71341=CARTESIAN_POINT('Ctrl Pts',(93.6893305019479,-4.77054318036337,340.123751140995));
#71342=CARTESIAN_POINT('Ctrl Pts',(93.411092467674,1.72705699629501,341.784407278614));
#71343=CARTESIAN_POINT('Ctrl Pts',(93.1328544333999,6.63976245877293,337.219112994336));
#71344=CARTESIAN_POINT('Ctrl Pts',(92.8546163991262,5.45925591556819,330.61737146921));
#71345=CARTESIAN_POINT('Ctrl Pts',(92.576378364852,-0.731129202868262,328.037503459299));
#71346=CARTESIAN_POINT('Ctrl Pts',(92.2981403305784,-6.25056784328173,331.847015758509));
#71347=CARTESIAN_POINT('Ctrl Pts',(92.0199022963041,-6.0339526321459,338.549975158163));
#71348=CARTESIAN_POINT('Ctrl Pts',(91.7416642620304,-0.28006815148484,341.995174752719));
#71349=CARTESIAN_POINT('Ctrl Pts',(91.4634262277564,5.73083073799484,339.021005725314));
#71350=CARTESIAN_POINT('Ctrl Pts',(91.1851881934825,6.48263084613968,332.356819093736));
#71351=CARTESIAN_POINT('Ctrl Pts',(90.9069501592086,1.28541631025659,328.118240566549));
#71352=CARTESIAN_POINT('Ctrl Pts',(90.6287121249346,-5.09140580083534,330.194951096839));
#71353=CARTESIAN_POINT('Ctrl Pts',(90.3504740906606,-6.79591995752712,336.681184083152));
#71354=CARTESIAN_POINT('Ctrl Pts',(90.0722360563868,-2.2639186768104,341.624619250595));
#71355=CARTESIAN_POINT('Ctrl Pts',(89.7939980221127,4.34564735823031,340.488739110985));
#71356=CARTESIAN_POINT('Ctrl Pts',(89.5157599878389,6.96727695427295,334.315924102882));
#71357=CARTESIAN_POINT('Ctrl Pts',(89.2375219535649,3.19513932621856,328.77087544862));
#71358=CARTESIAN_POINT('Ctrl Pts',(88.9592839192909,-3.50913050132744,328.942202453431));
#71359=CARTESIAN_POINT('Ctrl Pts',(88.6810458850171,-6.99312306248656,334.672680853784));
#71360=CARTESIAN_POINT('Ctrl Pts',(88.402807850743,-4.05962980752896,340.703535203396));
#71361=CARTESIAN_POINT('Ctrl Pts',(88.1245698164692,2.59932580176022,341.500339480894));
#71362=CARTESIAN_POINT('Ctrl Pts',(87.8463317821953,6.87291848876,336.331878161628));
#71363=CARTESIAN_POINT('Ctrl Pts',(87.5680937479212,4.83933532273533,329.941171911925));
#71364=CARTESIAN_POINT('Ctrl Pts',(87.2898557136474,-1.63523444049127,328.192877530469));
#71365=CARTESIAN_POINT('Ctrl Pts',(87.0116176793733,-6.60917369369981,332.691378966339));
#71366=CARTESIAN_POINT('Ctrl Pts',(86.7333796450995,-5.51797179944384,339.308467849607));
#71367=CARTESIAN_POINT('Ctrl Pts',(86.4551416108254,0.636991370031486,341.971739380174));
#71368=CARTESIAN_POINT('Ctrl Pts',(86.1769035765517,6.20739696120613,338.237148584259));
#71369=CARTESIAN_POINT('Ctrl Pts',(85.8986655422775,6.08136598211088,331.531874312804));
#71370=CARTESIAN_POINT('Ctrl Pts',(85.6204275080038,0.374555202047226,328.009247795038));
#71371=CARTESIAN_POINT('Ctrl Pts',(85.3421894737298,-5.67597935850943,330.901931392432));
#71372=CARTESIAN_POINT('Ctrl Pts',(85.0639514394557,-6.51775143908,337.555352063598));
#71373=CARTESIAN_POINT('Ctrl Pts',(84.7857134051819,-1.37827922586039,341.863763862935));
#71374=CARTESIAN_POINT('Ctrl Pts',(84.5074753709079,5.02601948956327,339.873400874245));
#71375=CARTESIAN_POINT('Ctrl Pts',(84.229237336634,6.81801430334078,333.41078983454));
#71376=CARTESIAN_POINT('Ctrl Pts',(83.9509993023601,2.35321802466861,328.406573506974));
#71377=CARTESIAN_POINT('Ctrl Pts',(83.6727612680862,-4.27109170180083,329.453047353243));
#71378=CARTESIAN_POINT('Ctrl Pts',(83.3945232338121,-6.97588361473783,335.589877770553));
#71379=CARTESIAN_POINT('Ctrl Pts',(83.1162851995383,-3.27901009830331,341.185386064409));
#71380=CARTESIAN_POINT('Ctrl Pts',(82.8380471652642,3.42696258723445,341.104656863105));
#71381=CARTESIAN_POINT('Ctrl Pts',(82.5598091309904,6.98806228835202,335.421774163117));
#71382=CARTESIAN_POINT('Ctrl Pts',(82.2815710967164,4.13632037107925,329.351835539013));
#71383=CARTESIAN_POINT('Ctrl Pts',(82.0033330624425,-2.51126169874435,328.465134073986));
#71384=CARTESIAN_POINT('Ctrl Pts',(81.7250950281686,-6.85429597379216,333.575382614799));
#71385=CARTESIAN_POINT('Ctrl Pts',(81.4468569938946,-4.90724400293366,339.992981502693));
#71386=CARTESIAN_POINT('Ctrl Pts',(81.1686189596206,1.5431133586142,341.828594961853));
#71387=CARTESIAN_POINT('Ctrl Pts',(80.8903809253469,6.57737836727761,337.397707614416));
#71388=CARTESIAN_POINT('Ctrl Pts',(80.6121428910727,5.57568033023622,330.766479379337));
#71389=CARTESIAN_POINT('Ctrl Pts',(80.3339048567989,-0.542737248956215,
328.020290531178));
#71390=CARTESIAN_POINT('Ctrl Pts',(80.0556668225249,-6.16309286557018,331.679278042214));
#71391=CARTESIAN_POINT('Ctrl Pts',(79.7774287882509,-6.12766912655199,338.385643080134));
#71392=CARTESIAN_POINT('Ctrl Pts',(79.4991907539772,-0.46897387434508,341.985053435425));
#71393=CARTESIAN_POINT('Ctrl Pts',(79.220952719703,5.62009178030527,339.174383352245));
#71394=CARTESIAN_POINT('Ctrl Pts',(78.9427146854293,6.55168216058818,332.532943280508));
#71395=CARTESIAN_POINT('Ctrl Pts',(78.6644766511551,1.47089052476949,328.15548474655));
#71396=CARTESIAN_POINT('Ctrl Pts',(78.3862386168814,-4.9597156353216,330.059136835804));
#71397=CARTESIAN_POINT('Ctrl Pts',(78.1080005826073,-6.83886396216083,336.49694612382));
#71398=CARTESIAN_POINT('Ctrl Pts',(77.8297625483334,-2.44208777239169,341.561030048895));
#71399=CARTESIAN_POINT('Ctrl Pts',(77.5515245140595,4.19575632094487,340.604153538743));
#71400=CARTESIAN_POINT('Ctrl Pts',(77.2732864797855,6.98321676781211,334.504428043259));
#71401=CARTESIAN_POINT('Ctrl Pts',(76.9950484455116,3.36228225896871,328.859481617845));
#71402=CARTESIAN_POINT('Ctrl Pts',(76.7168104112377,-3.34416905172548,328.849598277832));
#71403=CARTESIAN_POINT('Ctrl Pts',(76.4385723769637,-6.98172578350548,334.483847818472));
#71404=CARTESIAN_POINT('Ctrl Pts',(76.1603343426898,-4.21225581386615,340.591762597706));
#71405=CARTESIAN_POINT('Ctrl Pts',(75.8820963084158,2.42273914336425,341.568199375306));
#71406=CARTESIAN_POINT('Ctrl Pts',(75.6038582741419,6.83442214830042,336.517096532651));
#71407=CARTESIAN_POINT('Ctrl Pts',(75.3256202398679,4.97425682364685,330.07377659429));
#71408=CARTESIAN_POINT('Ctrl Pts',(75.0473822055941,-1.45071056815708,328.151179164411));
#71409=CARTESIAN_POINT('Ctrl Pts',(74.76914417132,-6.54438228401613,332.513643526922));
#71410=CARTESIAN_POINT('Ctrl Pts',(74.4909061370462,-5.63237097275777,339.157800526215));
#71411=CARTESIAN_POINT('Ctrl Pts',(74.2126681027722,0.448384046541121,341.986405351636));
#71412=CARTESIAN_POINT('Ctrl Pts',(73.9344300684983,6.1176636444669,338.403689105034));
#71413=CARTESIAN_POINT('Ctrl Pts',(73.6561920342243,6.17285361243278,331.697457605112));
#71414=CARTESIAN_POINT('Ctrl Pts',(73.3779539999505,0.563306931439073,328.021920515531));
#71415=CARTESIAN_POINT('Ctrl Pts',(73.0997159656764,-5.56317820613959,330.750063972565));
#71416=CARTESIAN_POINT('Ctrl Pts',(72.8214779314026,-6.58441681631968,337.378310993021));
#71417=CARTESIAN_POINT('Ctrl Pts',(72.5432398971284,-1.56323329999609,341.824017118996));
#71418=CARTESIAN_POINT('Ctrl Pts',(72.2650018628548,4.89250634244821,340.007423457194));
#71419=CARTESIAN_POINT('Ctrl Pts',(71.9867638285806,6.85846512770305,333.595591198175));
#71420=CARTESIAN_POINT('Ctrl Pts',(71.7085257943068,2.53051169604413,328.47256416755));
#71421=CARTESIAN_POINT('Ctrl Pts',(71.4302877600328,-4.11965496878306,329.339668655569));
#71422=CARTESIAN_POINT('Ctrl Pts',(71.1520497257589,-6.98927507476571,335.401175672019));
#71423=CARTESIAN_POINT('Ctrl Pts',(70.8738116914849,-3.44494060616687,341.094529695599));
#71424=CARTESIAN_POINT('Ctrl Pts',(70.595573657211,3.26076500947132,341.19502377264));
#71425=CARTESIAN_POINT('Ctrl Pts',(70.3173356229371,6.97411470473025,335.610435971929));
#71426=CARTESIAN_POINT('Ctrl Pts',(70.0390975886631,4.2874222732228,329.465660089801));
#71427=CARTESIAN_POINT('Ctrl Pts',(69.7608595543893,-2.33377429617208,328.399666256538));
#71428=CARTESIAN_POINT('Ctrl Pts',(69.4826215201152,-6.81330064042213,333.390701278884));
#71429=CARTESIAN_POINT('Ctrl Pts',(69.2043834858414,-5.04036155110939,339.858565984389));
#71430=CARTESIAN_POINT('Ctrl Pts',(68.9261454515673,1.3580429380419,341.867796398335));
#71431=CARTESIAN_POINT('Ctrl Pts',(68.6479074172935,6.51019146763303,337.57455142604));
#71432=CARTESIAN_POINT('Ctrl Pts',(68.3696693830195,5.6880333776459,330.918678610382));
#71433=CARTESIAN_POINT('Ctrl Pts',(68.0914313487456,-0.353948987771852,
328.008174193774));
#71434=CARTESIAN_POINT('Ctrl Pts',(67.8131933144717,-6.07111759138985,331.513965120359));
#71435=CARTESIAN_POINT('Ctrl Pts',(67.5349552801977,-6.21691119093816,338.2188388022));
#71436=CARTESIAN_POINT('Ctrl Pts',(67.2567172459238,-0.657537152021269,
341.969831625245));
#71437=CARTESIAN_POINT('Ctrl Pts',(66.9784792116499,5.50524902607308,339.324712840349));
#71438=CARTESIAN_POINT('Ctrl Pts',(66.7002411773758,6.61594943028259,332.710868914521));
#71439=CARTESIAN_POINT('Ctrl Pts',(66.422003143102,1.6552906935753,328.197726798318));
#71440=CARTESIAN_POINT('Ctrl Pts',(66.1437651088279,-4.82440388057547,329.92693039791));
#71441=CARTESIAN_POINT('Ctrl Pts',(65.8655270745542,-6.87681422160667,336.311615092955));
#71442=CARTESIAN_POINT('Ctrl Pts',(65.58728904028,-2.61847365308096,341.492649976603));
#71443=CARTESIAN_POINT('Ctrl Pts',(65.3090510060063,4.04280153826938,340.715475808078));
#71444=CARTESIAN_POINT('Ctrl Pts',(65.0308129717322,6.99405742960281,334.693293850764));
#71445=CARTESIAN_POINT('Ctrl Pts',(64.7525749374583,3.52697004990818,328.952571599629));
#71446=CARTESIAN_POINT('Ctrl Pts',(64.4743369031844,-3.17676568659459,328.761485131617));
#71447=CARTESIAN_POINT('Ctrl Pts',(64.1960988689105,-6.96523044149417,334.295391677991));
#71448=CARTESIAN_POINT('Ctrl Pts',(63.9178608346364,-4.36180602686735,340.475906881471));
#71449=CARTESIAN_POINT('Ctrl Pts',(63.6396228003626,2.2443833984642,341.631263164078));
#71450=CARTESIAN_POINT('Ctrl Pts',(63.3613847660885,6.79093530606982,336.701207118295));
#71451=CARTESIAN_POINT('Ctrl Pts',(63.0831467318148,5.10554611733597,330.209978409827));
#71452=CARTESIAN_POINT('Ctrl Pts',(62.8049086975407,-1.26512738553993,328.11448181406));
#71453=CARTESIAN_POINT('Ctrl Pts',(62.5266706632668,-6.47481215995544,332.337723627447));
#71454=CARTESIAN_POINT('Ctrl Pts',(62.2484326289928,-5.74265738325067,339.004097172791));
#71455=CARTESIAN_POINT('Ctrl Pts',(61.970194594719,0.259449312579205,341.995969843042));
#71456=CARTESIAN_POINT('Ctrl Pts',(61.6919565604449,6.02346320372072,338.567744248679));
#71457=CARTESIAN_POINT('Ctrl Pts',(61.4137185261711,6.25983381897889,331.865452417122));
#71458=CARTESIAN_POINT('Ctrl Pts',(61.1354804918971,0.751647333555837,328.039688636525));
#71459=CARTESIAN_POINT('Ctrl Pts',(60.8572424576232,-5.44631481557494,330.601299860162));
#71460=CARTESIAN_POINT('Ctrl Pts',(60.5790044233492,-6.64627424592751,337.199533277421));
#71461=CARTESIAN_POINT('Ctrl Pts',(60.3007663890754,-1.74704589963946,341.779287471048));
#71462=CARTESIAN_POINT('Ctrl Pts',(60.0225283548013,4.75542068239251,340.137789614614));
#71463=CARTESIAN_POINT('Ctrl Pts',(59.7442903205275,6.89390789408709,333.781418062499));
#71464=CARTESIAN_POINT('Ctrl Pts',(59.4660522862535,2.70595758529176,328.543321168189));
#71465=CARTESIAN_POINT('Ctrl Pts',(59.1878142519796,-3.96521005965715,329.230423137408));
#71466=CARTESIAN_POINT('Ctrl Pts',(58.9095762177056,-6.99756295926346,335.212180634613));
#71467=CARTESIAN_POINT('Ctrl Pts',(58.6313381834317,-3.60835561501372,340.999223095215));
#71468=CARTESIAN_POINT('Ctrl Pts',(58.3531001491577,3.09218641789253,341.280867069725));
#71469=CARTESIAN_POINT('Ctrl Pts',(58.0748621148839,6.95507461569553,335.798652039796));
#71470=CARTESIAN_POINT('Ctrl Pts',(57.7966240806098,4.43539349540778,329.583525821029));
#71471=CARTESIAN_POINT('Ctrl Pts',(57.518386046336,-2.15458276931499,328.339018009277));
#71472=CARTESIAN_POINT('Ctrl Pts',(57.240148012062,-6.76733022822695,333.207195054478));
#71473=CARTESIAN_POINT('Ctrl Pts',(56.961909977788,-5.16979862232547,339.720602736427));
#71474=CARTESIAN_POINT('Ctrl Pts',(56.6836719435141,1.17198087318151,341.901982963139));
#71475=CARTESIAN_POINT('Ctrl Pts',(56.4054339092402,6.43825081977916,337.74951529768));
#71476=CARTESIAN_POINT('Ctrl Pts',(56.1271958749663,5.7962330174918,331.073858026319));
#71477=CARTESIAN_POINT('Ctrl Pts',(55.8489578406922,-0.164902272688679,
328.001163294445));
#71478=CARTESIAN_POINT('Ctrl Pts',(55.5707198064184,-5.97470918117631,331.351197704598));
#71479=CARTESIAN_POINT('Ctrl Pts',(55.2924817721444,-6.3016136606614,338.049684125008));
#71480=CARTESIAN_POINT('Ctrl Pts',(55.0142437378705,-0.845620295422691,
341.949520437162));
#71481=CARTESIAN_POINT('Ctrl Pts',(54.7360057035965,5.38638633359033,339.471884418886));
#71482=CARTESIAN_POINT('Ctrl Pts',(54.4577676693226,6.67538572719945,332.890466074303));
#71483=CARTESIAN_POINT('Ctrl Pts',(54.1795296350486,1.83848216748947,328.244935876664));
#71484=CARTESIAN_POINT('Ctrl Pts',(53.9012916007747,-4.68556934137328,329.798428320426));
#71485=CARTESIAN_POINT('Ctrl Pts',(53.6230535665008,-6.9097430245479,336.125326319462));
#71486=CARTESIAN_POINT('Ctrl Pts',(53.3448155322269,-2.79294752173477,341.419528964915));
#71487=CARTESIAN_POINT('Ctrl Pts',(53.0665774979529,3.88689469793651,340.82262463136));
#71488=CARTESIAN_POINT('Ctrl Pts',(52.788339463679,6.99979102378316,334.882383615403));
#71489=CARTESIAN_POINT('Ctrl Pts',(52.510101429405,3.68908244385015,329.050077419576));
#71490=CARTESIAN_POINT('Ctrl Pts',(52.2318633951311,-3.00704264403653,328.677927355091));
#71491=CARTESIAN_POINT('Ctrl Pts',(51.9536253608571,-6.94364908136755,334.107450043199));
#71492=CARTESIAN_POINT('Ctrl Pts',(51.6753873265832,-4.50817124482002,340.356052652648));
#71493=CARTESIAN_POINT('Ctrl Pts',(51.3971492923092,2.06438880260035,341.689484797969));
#71494=CARTESIAN_POINT('Ctrl Pts',(51.1189112580354,6.74248971620314,336.884075480828));
#71495=CARTESIAN_POINT('Ctrl Pts',(50.8406732237614,5.23310733623141,330.349677903839));
#71496=CARTESIAN_POINT('Ctrl Pts',(50.5624351894875,-1.07862040566223,328.082812275856));
#71497=CARTESIAN_POINT('Ctrl Pts',(50.2841971552135,-6.40051412169072,332.163747724796));
#71498=CARTESIAN_POINT('Ctrl Pts',(50.0059591209396,-5.84875049967723,338.847470023676));
#71499=CARTESIAN_POINT('Ctrl Pts',(49.7277210866656,0.0703251284742021,
342.000425870393));
#71500=CARTESIAN_POINT('Ctrl Pts',(49.4494830523918,5.92486442422205,338.729194221966));
#71501=CARTESIAN_POINT('Ctrl Pts',(49.1712450181177,6.34224308871686,332.035736078859));
#71502=CARTESIAN_POINT('Ctrl Pts',(48.8930069838439,0.939438882050772,328.062539183717));
#71503=CARTESIAN_POINT('Ctrl Pts',(48.6147689495699,-5.32547452057817,330.455747682926));
#71504=CARTESIAN_POINT('Ctrl Pts',(48.336530915296,-6.70327855954755,337.019149460459));
#71505=CARTESIAN_POINT('Ctrl Pts',(48.058292881022,-1.9295828046498,341.729607580726));
#71506=CARTESIAN_POINT('Ctrl Pts',(47.7800548467481,4.61486260947957,340.264404153007));
#71507=CARTESIAN_POINT('Ctrl Pts',(47.5018168124742,6.92431672215013,333.968134736551));
#71508=CARTESIAN_POINT('Ctrl Pts',(47.2235787782002,2.8794275816508,328.618792842057));
#71509=CARTESIAN_POINT('Ctrl Pts',(46.9453407439263,-3.80786975024803,329.125390569943));
#71510=CARTESIAN_POINT('Ctrl Pts',(46.6671027096523,-7.00074121640962,335.023030662701));
#71511=CARTESIAN_POINT('Ctrl Pts',(46.3888646753784,-3.76913579904309,340.899535856229));
#71512=CARTESIAN_POINT('Ctrl Pts',(46.1106266411045,2.92134990875209,341.362124071503));
#71513=CARTESIAN_POINT('Ctrl Pts',(45.8323886068305,6.93095592433945,335.986284931156));
#71514=CARTESIAN_POINT('Ctrl Pts',(45.5541505725566,4.58012598890224,329.705346667029));
#71515=CARTESIAN_POINT('Ctrl Pts',(45.2759125382826,-1.97381796400176,328.283233617615));
#71516=CARTESIAN_POINT('Ctrl Pts',(44.9976745040087,-6.71641830484675,333.024997938006));
#71517=CARTESIAN_POINT('Ctrl Pts',(44.7194364697347,-5.29546070150554,339.579192499707));
#71518=CARTESIAN_POINT('Ctrl Pts',(44.4411984354609,0.985063026735457,341.931129693197));
#71519=CARTESIAN_POINT('Ctrl Pts',(44.1629604011869,6.36160895484778,337.922471470547));
#71520=CARTESIAN_POINT('Ctrl Pts',(43.884722366913,5.90020024229054,331.231904314985));
#71521=CARTESIAN_POINT('Ctrl Pts',(43.606484332639,0.0242648541961058,327.999262952559));
#71522=CARTESIAN_POINT('Ctrl Pts',(43.3282462983651,-5.87393803244544,331.191094647862));
#71523=CARTESIAN_POINT('Ctrl Pts',(43.0500082640912,-6.38171468589505,337.87830256547));
#71524=CARTESIAN_POINT('Ctrl Pts',(42.7717702298172,-1.03308596605334,341.924134702423));
#71525=CARTESIAN_POINT('Ctrl Pts',(42.4935321955433,5.2635904965114,339.615790623024));
#71526=CARTESIAN_POINT('Ctrl Pts',(42.2152941612694,6.72994765089654,333.071603617833));
#71527=CARTESIAN_POINT('Ctrl Pts',(41.9370561269954,2.02033117991846,328.297077509473));
#71528=CARTESIAN_POINT('Ctrl Pts',(41.6588180927215,-4.54331339483144,329.673724435696));
#71529=CARTESIAN_POINT('Ctrl Pts',(41.3805800584475,-6.93762632634033,335.938215831582));
#71530=CARTESIAN_POINT('Ctrl Pts',(41.1023420241736,-2.96538197736341,341.341720406868));
#71531=CARTESIAN_POINT('Ctrl Pts',(40.8241039898996,3.72814964327367,340.925521768411));
#71532=CARTESIAN_POINT('Ctrl Pts',(40.5458659556258,7.00041336367703,335.071559263642));
#71533=CARTESIAN_POINT('Ctrl Pts',(40.2676279213517,3.84850106616587,329.15192787884));
#71534=CARTESIAN_POINT('Ctrl Pts',(39.9893898870779,-2.8351238559831,328.598985962225));
#71535=CARTESIAN_POINT('Ctrl Pts',(39.7111518528039,-6.91699746185588,333.920160149263));
#71536=CARTESIAN_POINT('Ctrl Pts',(39.43291381853,-4.65124459169871,340.232287428912));
#71537=CARTESIAN_POINT('Ctrl Pts',(39.154675784256,1.88288678800273,341.742821763484));
#71538=CARTESIAN_POINT('Ctrl Pts',(38.8764377499821,6.68912075371751,337.065568089594));
#71539=CARTESIAN_POINT('Ctrl Pts',(38.5981997157081,5.35684733500621,330.492773067617));
#71540=CARTESIAN_POINT('Ctrl Pts',(38.3199616814342,-0.891325816103229,
328.056193674929));
#71541=CARTESIAN_POINT('Ctrl Pts',(38.0417236471602,-6.32154242172221,331.991842856344));
#71542=CARTESIAN_POINT('Ctrl Pts',(37.7634856128864,-5.95057285273992,338.688033448167));
#71543=CARTESIAN_POINT('Ctrl Pts',(37.4852475786124,-0.118850407109541,
341.999770179891));
#71544=CARTESIAN_POINT('Ctrl Pts',(37.2070095443385,5.82193930289614,338.887921133968));
#71545=CARTESIAN_POINT('Ctrl Pts',(36.9287715100645,6.42002124631727,332.208184249024));
#71546=CARTESIAN_POINT('Ctrl Pts',(36.6505334757906,1.12654445135132,328.090455471618));
#71547=CARTESIAN_POINT('Ctrl Pts',(36.3722954415166,-5.2007455588509,330.313513723198));
#71548=CARTESIAN_POINT('Ctrl Pts',(36.0940574072427,-6.75538813257426,336.837291258574));
#71549=CARTESIAN_POINT('Ctrl Pts',(35.8158193729687,-2.11071072639963,341.675013724332));
#71550=CARTESIAN_POINT('Ctrl Pts',(35.5375813386949,4.4709347593527,340.38717461831));
#71551=CARTESIAN_POINT('Ctrl Pts',(35.2593433044208,6.94966940733592,334.155604879633));
#71552=CARTESIAN_POINT('Ctrl Pts',(34.981105270147,3.05079501715928,328.698924079665));
#71553=CARTESIAN_POINT('Ctrl Pts',(34.702867235873,-3.64774893060379,329.024647648059));
#71554=CARTESIAN_POINT('Ctrl Pts',(34.4246292015991,-6.99880752543772,334.833863873775));
#71555=CARTESIAN_POINT('Ctrl Pts',(34.1463911673251,-3.9271637564072,340.795540770361));
#71556=CARTESIAN_POINT('Ctrl Pts',(33.8681531330512,2.74838022703619,341.43873544403));
#71557=CARTESIAN_POINT('Ctrl Pts',(33.5899150987772,6.90177624215411,336.17319763629));
#71558=CARTESIAN_POINT('Ctrl Pts',(33.3116770645033,4.72151406989757,329.831033674098));
#71559=CARTESIAN_POINT('Ctrl Pts',(33.0334390302294,-1.79161187487054,328.232353815365));
#71560=CARTESIAN_POINT('Ctrl Pts',(32.7552009959554,-6.66060204621789,332.844242969981));
#71561=CARTESIAN_POINT('Ctrl Pts',(32.4769629616815,-5.41725603007612,339.43443853212));
#71562=CARTESIAN_POINT('Ctrl Pts',(32.1987249274076,0.79742588629856,341.955215305542));
#71563=CARTESIAN_POINT('Ctrl Pts',(31.9204868931336,6.28032183680384,338.093293651873));
#71564=CARTESIAN_POINT('Ctrl Pts',(31.6422488588597,5.9998591350726,331.392702070823));
#71565=CARTESIAN_POINT('Ctrl Pts',(31.3640108245857,0.213414262860903,328.002474555747));
#71566=CARTESIAN_POINT('Ctrl Pts',(31.0857727903118,-5.76887772838889,331.033772857557));
#71567=CARTESIAN_POINT('Ctrl Pts',(30.8075347560379,-6.4571557767919,337.704819266569));
#71568=CARTESIAN_POINT('Ctrl Pts',(30.5292967217639,-1.21979727629601,341.89369295772));
#71569=CARTESIAN_POINT('Ctrl Pts',(30.25105868749,5.13695118047843,339.756326372311));
#71570=CARTESIAN_POINT('Ctrl Pts',(29.9728206532161,6.77959536020297,333.254149278297));
#71571=CARTESIAN_POINT('Ctrl Pts',(29.6945826189421,2.20070494453272,328.354113622873));
#71572=CARTESIAN_POINT('Ctrl Pts',(29.4163445846682,-4.39773991638346,329.55290980262));
#71573=CARTESIAN_POINT('Ctrl Pts',(29.1381065503942,-6.9604437665693,335.75042025758));
#71574=CARTESIAN_POINT('Ctrl Pts',(28.8598685161203,-3.13565110815609,341.259281118346));
#71575=CARTESIAN_POINT('Ctrl Pts',(28.5816304818463,3.56668229007748,341.024092083642));
#71576=CARTESIAN_POINT('Ctrl Pts',(28.3033924475724,6.99592399485125,335.260682659234));
#71577=CARTESIAN_POINT('Ctrl Pts',(28.0251544132985,4.00510950921894,329.258048606115));
#71578=CARTESIAN_POINT('Ctrl Pts',(27.7469163790245,-2.66113485770415,328.524718596103));
#71579=CARTESIAN_POINT('Ctrl Pts',(27.4686783447506,-6.88529504399824,333.733658755447));
#71580=CARTESIAN_POINT('Ctrl Pts',(27.1904403104767,-4.79092159520341,340.104701583755));
#71581=CARTESIAN_POINT('Ctrl Pts',(26.9122022762027,1.70000988762276,341.79123511392));
#71582=CARTESIAN_POINT('Ctrl Pts',(26.6339642419288,6.63086738868234,337.245552418509));
#71583=CARTESIAN_POINT('Ctrl Pts',(26.3557262076548,5.47667575859036,330.639159412931));
#71584=CARTESIAN_POINT('Ctrl Pts',(26.077488173381,-0.7033803795583,328.034645448205));
#71585=CARTESIAN_POINT('Ctrl Pts',(25.7992501391069,-6.23795472526369,331.822134547197));
#71586=CARTESIAN_POINT('Ctrl Pts',(25.5210121048331,-6.04805009165541,338.525903867009));
#71587=CARTESIAN_POINT('Ctrl Pts',(25.2427740705591,-0.307939158007984,
341.994003250322));
#71588=CARTESIAN_POINT('Ctrl Pts',(24.9645360362852,5.71476299576885,339.043809082135));
#71589=CARTESIAN_POINT('Ctrl Pts',(24.6862980020112,6.49311149809216,332.382671005795));
#71590=CARTESIAN_POINT('Ctrl Pts',(24.4080599677373,1.31282741678491,328.123417115725));
#71591=CARTESIAN_POINT('Ctrl Pts',(24.1298219334633,-5.07221900760495,330.174701840357));
#71592=CARTESIAN_POINT('Ctrl Pts',(23.8515838991894,-6.80256491454558,336.654091464809));
#71593=CARTESIAN_POINT('Ctrl Pts',(23.5733458649154,-2.29029740510129,341.615545766355));
#71594=CARTESIAN_POINT('Ctrl Pts',(23.2951078306416,4.32374222827016,340.506011363414));
#71595=CARTESIAN_POINT('Ctrl Pts',(23.0168697963675,6.96994743708876,334.34369160086));
#71596=CARTESIAN_POINT('Ctrl Pts',(22.7386317620937,3.21993475914654,328.783656369104));
#71597=CARTESIAN_POINT('Ctrl Pts',(22.4603937278197,-3.48496452110532,328.928267934336));
#71598=CARTESIAN_POINT('Ctrl Pts',(22.1821556935458,-6.99176329833085,334.644818397613));
#71599=CARTESIAN_POINT('Ctrl Pts',(21.9039176592718,-4.08232409493527,340.687313774926));
#71600=CARTESIAN_POINT('Ctrl Pts',(21.6256796249979,2.57340367537753,341.510645245605));
#71601=CARTESIAN_POINT('Ctrl Pts',(21.3474415907239,6.86755687617236,336.359253671357));
#71602=CARTESIAN_POINT('Ctrl Pts',(21.06920355645,4.85945449667722,329.960495065457));
#71603=CARTESIAN_POINT('Ctrl Pts',(20.7909655221761,-1.6080975489873,328.186415755015));
#71604=CARTESIAN_POINT('Ctrl Pts',(20.5127274879022,-6.59992220942738,332.665062137858));
#71605=CARTESIAN_POINT('Ctrl Pts',(20.2344894536283,-5.53509567296828,339.286446533161));
#71606=CARTESIAN_POINT('Ctrl Pts',(19.9562514193543,0.609206464695599,341.974222212831));
#71607=CARTESIAN_POINT('Ctrl Pts',(19.6780133850804,6.19444882158101,338.261857107137));
#71608=CARTESIAN_POINT('Ctrl Pts',(19.3997753508064,6.09513692481626,331.556133879155));
#71609=CARTESIAN_POINT('Ctrl Pts',(19.1215373165325,0.40240783622117,328.010795758893));
#71610=CARTESIAN_POINT('Ctrl Pts',(18.8432992822585,-5.65960498414416,330.87934721021));
#71611=CARTESIAN_POINT('Ctrl Pts',(18.5650612479846,-6.52788184619303,337.529360905981));
#71612=CARTESIAN_POINT('Ctrl Pts',(18.2868232137106,-1.40561788936867,341.85821743164));
#71613=CARTESIAN_POINT('Ctrl Pts',(18.0085851794367,5.00656085764329,339.893389047406));
#71614=CARTESIAN_POINT('Ctrl Pts',(17.7303471451628,6.82429260231311,333.437969760673));
#71615=CARTESIAN_POINT('Ctrl Pts',(17.4521091108888,2.3794717522339,328.41600256904));
#71616=CARTESIAN_POINT('Ctrl Pts',(17.1738710766149,-4.24895520392486,329.436072640157));
#71617=CARTESIAN_POINT('Ctrl Pts',(16.895633042341,-6.97817868391783,335.562076725969));
#71618=CARTESIAN_POINT('Ctrl Pts',(16.617395008067,-3.30363058342786,341.172271296598));
#71619=CARTESIAN_POINT('Ctrl Pts',(16.3391569737931,3.40261054196623,341.118263600914));
#71620=CARTESIAN_POINT('Ctrl Pts',(16.0609189395192,6.98632619544743,335.449615704094));
#71621=CARTESIAN_POINT('Ctrl Pts',(15.7826809052452,4.15879341737169,329.368362111944));
#71622=CARTESIAN_POINT('Ctrl Pts',(15.5044428709713,-2.48520269613499,328.455179486824));
#71623=CARTESIAN_POINT('Ctrl Pts',(15.2262048366973,-6.84856497693183,333.548082045253));
#71624=CARTESIAN_POINT('Ctrl Pts',(14.9479668024234,-4.92710026304873,339.973388280481));
#71625=CARTESIAN_POINT('Ctrl Pts',(14.6697287681495,1.51589163834792,341.834689497799));
#71626=CARTESIAN_POINT('Ctrl Pts',(14.3914907338755,6.56777215776715,337.423897042843));
#71627=CARTESIAN_POINT('Ctrl Pts',(14.1132526996016,5.59250510814167,330.788730048326));
#71628=CARTESIAN_POINT('Ctrl Pts',(13.8350146653276,-0.514921333947683,
328.018183330228));
#71629=CARTESIAN_POINT('Ctrl Pts',(13.5567766310537,-6.14981206817078,331.654746718514));
#71630=CARTESIAN_POINT('Ctrl Pts',(13.2785385967797,-6.14111103837664,338.361199667403));
#71631=CARTESIAN_POINT('Ctrl Pts',(13.0003005625058,-0.496803051568086,
341.983129292665));
#71632=CARTESIAN_POINT('Ctrl Pts',(12.7220625282319,5.60341376334212,339.196744237014));
#71633=CARTESIAN_POINT('Ctrl Pts',(12.443824493958,6.56146047298106,332.559068938624));
#71634=CARTESIAN_POINT('Ctrl Pts',(12.165586459684,1.49815175526964,328.161400047695));
#71635=CARTESIAN_POINT('Ctrl Pts',(11.8873484254101,-4.93998871879135,330.039413394447));
#71636=CARTESIAN_POINT('Ctrl Pts',(11.6091103911361,-6.84477445364715,336.469683852826));
#71637=CARTESIAN_POINT('Ctrl Pts',(11.3308723568622,-2.46821171258475,341.551247128476));
#71638=CARTESIAN_POINT('Ctrl Pts',(11.0526343225883,4.17339250806404,340.620827617158));
#71639=CARTESIAN_POINT('Ctrl Pts',(10.7743962883143,6.98513598227502,334.532257552422));
#71640=CARTESIAN_POINT('Ctrl Pts',(10.4961582540404,3.3867233433309,328.872927851433));
#71641=CARTESIAN_POINT('Ctrl Pts',(10.2179202197665,-3.31963546586816,328.836321781429));
#71642=CARTESIAN_POINT('Ctrl Pts',(9.9396821854925,-6.97961353003579,334.456032320548));
#71643=CARTESIAN_POINT('Ctrl Pts',(9.66144415121862,-4.23450379727599,340.574933812142));
#71644=CARTESIAN_POINT('Ctrl Pts',(9.38320611694463,2.39654855218155,341.577801128574));
#71645=CARTESIAN_POINT('Ctrl Pts',(9.10496808267072,6.82832181198693,336.544316874147));
#71646=CARTESIAN_POINT('Ctrl Pts',(8.82673004839677,4.9938484358946,330.09363688212));
#71647=CARTESIAN_POINT('Ctrl Pts',(8.54849201412284,-1.4234125590739,328.145451897039));
#71648=CARTESIAN_POINT('Ctrl Pts',(8.2702539798489,-6.53441636134746,332.487588325599));
#71649=CARTESIAN_POINT('Ctrl Pts',(7.99201594557494,-5.64890631307911,339.135320703576));
#71650=CARTESIAN_POINT('Ctrl Pts',(7.71377791130103,0.420566235859593,341.988143830623));
#71651=CARTESIAN_POINT('Ctrl Pts',(7.43553987702708,6.1040072290099,338.428024977785));
#71652=CARTESIAN_POINT('Ctrl Pts',(7.15730184275314,6.18604973530199,331.722106408789));
#71653=CARTESIAN_POINT('Ctrl Pts',(6.8790638084792,0.590945759089165,328.024171379594));
#71654=CARTESIAN_POINT('Ctrl Pts',(6.60082577420527,-5.54589404922238,330.728023190032));
#71655=CARTESIAN_POINT('Ctrl Pts',(6.32258773993133,-6.59441823814528,337.351880525878));
#71656=CARTESIAN_POINT('Ctrl Pts',(6.04434970565737,-1.58932212683603,341.818064601347));
#71657=CARTESIAN_POINT('Ctrl Pts',(5.76611167138347,4.87045235443919,340.026254453026));
#71658=CARTESIAN_POINT('Ctrl Pts',(5.48787363710948,6.86793575564766,333.624108657021));
#71659=CARTESIAN_POINT('Ctrl Pts',(5.20963560283559,2.5487975662465,328.480480750959));
#71660=CARTESIAN_POINT('Ctrl Pts',(4.97777057427396,-2.97535607058049,329.186249754624));
#71661=CARTESIAN_POINT('Ctrl Pts',(4.79227855142465,-5.56135735959864,332.348719775238));
#71662=CARTESIAN_POINT('Ctrl Pts',(4.69953254000002,-5.96441153797609,334.331397335507));
#71663=CARTESIAN_POINT('Ctrl Pts',(4.65315953428771,-5.9118477353294,335.315703728026));
#71664=CARTESIAN_POINT('Ctrl Pts',(5.23167681249931,2.54972650148121,329.651773033606));
#71665=CARTESIAN_POINT('Ctrl Pts',(5.23167681249913,2.41800456025,329.600786237743));
#71666=CARTESIAN_POINT('Ctrl Pts',(5.23167681249913,2.28466063361559,329.554959909234));
#71667=CARTESIAN_POINT('Ctrl Pts',(5.23167681249924,2.14986992676735,329.514508295526));
#71668=CARTESIAN_POINT('Ctrl Pts',(5.23167681249934,1.9939798467528,329.467724615515));
#71669=CARTESIAN_POINT('Ctrl Pts',(5.23167681249914,1.83615434792712,329.428128731723));
#71670=CARTESIAN_POINT('Ctrl Pts',(5.23167681249919,1.67684153369454,329.39557219129));
#71671=CARTESIAN_POINT('Ctrl Pts',(5.23167681249925,1.51476829684993,329.362451541745));
#71672=CARTESIAN_POINT('Ctrl Pts',(5.23167681249897,1.3511549534905,329.336616380309));
#71673=CARTESIAN_POINT('Ctrl Pts',(5.23167681249917,1.18647141068386,329.317964639992));
#71674=CARTESIAN_POINT('Ctrl Pts',(5.23167681249938,1.02229982133636,329.299370882536));
#71675=CARTESIAN_POINT('Ctrl Pts',(5.23167681249934,0.857063874684294,329.287916213189));
#71676=CARTESIAN_POINT('Ctrl Pts',(5.23167681249924,0.69123933862632,329.283550047204));
#71677=CARTESIAN_POINT('Ctrl Pts',(5.23167681249917,0.60435650777413,329.28126241915));
#71678=CARTESIAN_POINT('Ctrl Pts',(5.23167681249934,0.517312342263204,329.280921526507));
#71679=CARTESIAN_POINT('Ctrl Pts',(5.23167681249914,0.430177521044325,329.282525300652));
#71680=CARTESIAN_POINT('Ctrl Pts',(5.23167681249905,0.404341844458899,329.283000823406));
#71681=CARTESIAN_POINT('Ctrl Pts',(5.23167681249918,0.378498210928564,329.283647332065));
#71682=CARTESIAN_POINT('Ctrl Pts',(5.23167681249927,0.352648497412946,329.28446483084));
#71683=CARTESIAN_POINT('Ctrl Pts',(5.23167681249934,0.333502347151716,329.285070329016));
#71684=CARTESIAN_POINT('Ctrl Pts',(5.23167681249895,0.314356581885818,329.285769540827));
#71685=CARTESIAN_POINT('Ctrl Pts',(5.23167681249896,0.29522010113727,329.286561951824));
#71686=CARTESIAN_POINT('Ctrl Pts',(5.23167681249928,0.132424129356062,329.293303072094));
#71687=CARTESIAN_POINT('Ctrl Pts',(5.23167681249911,-0.0298768216824351,
329.306790091531));
#71688=CARTESIAN_POINT('Ctrl Pts',(5.23167681249905,-0.191242176401267,
329.326890528971));
#71689=CARTESIAN_POINT('Ctrl Pts',(5.23167681249897,-0.352490232216596,
329.346976355101));
#71690=CARTESIAN_POINT('Ctrl Pts',(5.23167681249913,-0.512804836598123,
329.373666256176));
#71691=CARTESIAN_POINT('Ctrl Pts',(5.231676812499,-0.671735302422305,329.406878795084));
#71692=CARTESIAN_POINT('Ctrl Pts',(5.23167681249886,-0.829399809068293,
329.439826779817));
#71693=CARTESIAN_POINT('Ctrl Pts',(5.23167681249914,-0.985702858372395,
329.479194206026));
#71694=CARTESIAN_POINT('Ctrl Pts',(5.23167681249911,-1.14018237932099,329.524947201073));
#71695=CARTESIAN_POINT('Ctrl Pts',(5.23167681249913,-1.29176664913119,329.569842694685));
#71696=CARTESIAN_POINT('Ctrl Pts',(5.23167681249886,-1.44159568927443,329.620886982488));
#71697=CARTESIAN_POINT('Ctrl Pts',(5.23167681249887,-1.58920207264907,329.6780873439));
#71698=CARTESIAN_POINT('Ctrl Pts',(5.23167681249886,-1.63376575171165,329.695356641406));
#71699=CARTESIAN_POINT('Ctrl Pts',(5.23167681249898,-1.67812658882095,329.713187315508));
#71700=CARTESIAN_POINT('Ctrl Pts',(5.23167681249908,-1.72227103140139,329.731580219596));
#71701=CARTESIAN_POINT('Ctrl Pts',(5.23167681249914,-1.74269662266794,329.740090598687));
#71702=CARTESIAN_POINT('Ctrl Pts',(5.23167681249896,-1.76307588106098,329.748721349947));
#71703=CARTESIAN_POINT('Ctrl Pts',(5.23167681249893,-1.78340743812514,329.757472579012));
#71704=CARTESIAN_POINT('Ctrl Pts',(5.2316768124989,-1.80175923588897,329.765371668367));
#71705=CARTESIAN_POINT('Ctrl Pts',(5.23167681249882,-1.82006330253293,329.773365104279));
#71706=CARTESIAN_POINT('Ctrl Pts',(5.2316768124988,-1.83831746521071,329.781452110194));
#71707=CARTESIAN_POINT('Ctrl Pts',(5.23167681249883,-1.98233092296423,329.845253321194));
#71708=CARTESIAN_POINT('Ctrl Pts',(5.23167681249912,-2.12326805205457,329.914886745487));
#71709=CARTESIAN_POINT('Ctrl Pts',(5.23167681249902,-2.26071365305021,329.990282849218));
#71710=CARTESIAN_POINT('Ctrl Pts',(5.23167681249892,-2.39524127464768,330.064078288571));
#71711=CARTESIAN_POINT('Ctrl Pts',(5.23167681249882,-2.52642458879079,330.143394699649));
#71712=CARTESIAN_POINT('Ctrl Pts',(5.2316768124988,-2.65384554720594,330.228206595191));
#71713=CARTESIAN_POINT('Ctrl Pts',(5.23167681249879,-2.78009118683411,330.312236193885));
#71714=CARTESIAN_POINT('Ctrl Pts',(5.23167681249893,-2.90264409733492,330.401660629697));
#71715=CARTESIAN_POINT('Ctrl Pts',(5.23167681249907,-3.02106112099374,330.496489900504));
#71716=CARTESIAN_POINT('Ctrl Pts',(5.23167681249913,-3.06951763393609,330.535294251823));
#71717=CARTESIAN_POINT('Ctrl Pts',(5.23167681249888,-3.11728113419466,330.575004008348));
#71718=CARTESIAN_POINT('Ctrl Pts',(5.23167681249888,-3.16431914920114,330.615621404147));
#71719=CARTESIAN_POINT('Ctrl Pts',(5.23167681249886,-3.24767930945342,330.687603026296));
#71720=CARTESIAN_POINT('Ctrl Pts',(5.23167681249914,-3.32876163279295,330.762435095702));
#71721=CARTESIAN_POINT('Ctrl Pts',(5.23167681249899,-3.4074669648841,330.839968817051));
#71722=CARTESIAN_POINT('Ctrl Pts',(5.23167681249894,-3.43520704029975,330.867295952587));
#71723=CARTESIAN_POINT('Ctrl Pts',(5.23167681249884,-3.46265172518095,330.894958735291));
#71724=CARTESIAN_POINT('Ctrl Pts',(5.23167681249889,-3.48979631081915,330.92295075014));
#71725=CARTESIAN_POINT('Ctrl Pts',(5.23167681249892,-3.50731669470894,330.941018104438));
#71726=CARTESIAN_POINT('Ctrl Pts',(5.2316768124991,-3.52471423933795,330.959225054822));
#71727=CARTESIAN_POINT('Ctrl Pts',(5.23167681249907,-3.54197006666573,330.977550883116));
#71728=CARTESIAN_POINT('Ctrl Pts',(5.23167681249883,-3.64657636679153,331.088643620552));
#71729=CARTESIAN_POINT('Ctrl Pts',(5.23167681249895,-3.74611177326817,331.204237309737));
#71730=CARTESIAN_POINT('Ctrl Pts',(5.23167681249889,-3.84040442081676,331.323872703633));
#71731=CARTESIAN_POINT('Ctrl Pts',(5.23167681249883,-3.9352794679761,331.444247026901));
#71732=CARTESIAN_POINT('Ctrl Pts',(5.23167681249906,-4.02484714647093,331.568713946577));
#71733=CARTESIAN_POINT('Ctrl Pts',(5.23167681249906,-4.10888757179936,331.696834186031));
#71734=CARTESIAN_POINT('Ctrl Pts',(5.23167681249907,-4.19217159231138,331.823801280843));
#71735=CARTESIAN_POINT('Ctrl Pts',(5.23167681249912,-4.27002763524665,331.954357048025));
#71736=CARTESIAN_POINT('Ctrl Pts',(5.23167681249907,-4.34219365759432,332.08808963197));
#71737=CARTESIAN_POINT('Ctrl Pts',(5.23167681249902,-4.40188475268049,332.198704629509));
#71738=CARTESIAN_POINT('Ctrl Pts',(5.23167681249893,-4.45768221768303,332.311493540761));
#71739=CARTESIAN_POINT('Ctrl Pts',(5.23167681249896,-4.50941085668205,332.426225627016));
#71740=CARTESIAN_POINT('Ctrl Pts',(5.23167681249896,-4.53597814258197,332.485150821965));
#71741=CARTESIAN_POINT('Ctrl Pts',(5.23167681249895,-4.56147177056669,332.54458857805));
#71742=CARTESIAN_POINT('Ctrl Pts',(5.23167681249904,-4.58586534653017,332.604507433144));
#71743=CARTESIAN_POINT('Ctrl Pts',(5.23167681249908,-4.59440157528401,332.625475291834));
#71744=CARTESIAN_POINT('Ctrl Pts',(5.23167681249906,-4.60280385876661,332.646504055389));
#71745=CARTESIAN_POINT('Ctrl Pts',(5.23167681249904,-4.61106852320073,332.667586003979));
#71746=CARTESIAN_POINT('Ctrl Pts',(5.23167681249897,-4.62531373153314,332.703923444186));
#71747=CARTESIAN_POINT('Ctrl Pts',(5.23167681249907,-4.63914236795992,332.740398919073));
#71748=CARTESIAN_POINT('Ctrl Pts',(5.23167681249909,-4.65255058106541,332.77700510479));
#71749=CARTESIAN_POINT('Ctrl Pts',(5.23167681249902,-4.70421003064279,332.918042198278));
#71750=CARTESIAN_POINT('Ctrl Pts',(5.23167681249893,-4.74963264388488,333.061019116744));
#71751=CARTESIAN_POINT('Ctrl Pts',(5.23167681249899,-4.78874025475357,333.205562400287));
#71752=CARTESIAN_POINT('Ctrl Pts',(5.23167681249905,-4.82772255338508,333.349642524823));
#71753=CARTESIAN_POINT('Ctrl Pts',(5.23167681249904,-4.86043026958429,333.495279716321));
#71754=CARTESIAN_POINT('Ctrl Pts',(5.23167681249911,-4.88673444228786,333.642104028461));
#71755=CARTESIAN_POINT('Ctrl Pts',(5.2316768124991,-4.8986962336663,333.708872210487));
#71756=CARTESIAN_POINT('Ctrl Pts',(5.23167681249901,-4.90933308743962,333.775885817694));
#71757=CARTESIAN_POINT('Ctrl Pts',(5.23167681249898,-4.91862931835759,333.843109441235));
#71758=CARTESIAN_POINT('Ctrl Pts',(5.23167681249898,-4.92292145082778,333.874147041302));
#71759=CARTESIAN_POINT('Ctrl Pts',(5.23167681249906,-4.92692776730969,333.90522940348));
#71760=CARTESIAN_POINT('Ctrl Pts',(5.23167681249906,-4.9306465628392,333.936352997078));
#71761=CARTESIAN_POINT('Ctrl Pts',(5.23167681249907,-4.93342662939924,333.959620117064));
#71762=CARTESIAN_POINT('Ctrl Pts',(5.23167681249907,-4.93604591532386,333.98291004826));
#71763=CARTESIAN_POINT('Ctrl Pts',(5.23167681249907,-4.93850239243566,334.006207207835));
#71764=CARTESIAN_POINT('Ctrl Pts',(5.23167681249908,-4.95383544263047,334.151625422982));
#71765=CARTESIAN_POINT('Ctrl Pts',(5.23167681249901,-4.96284677660462,334.297465472424));
#71766=CARTESIAN_POINT('Ctrl Pts',(5.23167681249902,-4.96543576666754,334.44337495279));
#71767=CARTESIAN_POINT('Ctrl Pts',(5.23167681249896,-4.96798156936119,334.5868504931));
#71768=CARTESIAN_POINT('Ctrl Pts',(5.231676812499,-4.96431738792226,334.730393784283));
#71769=CARTESIAN_POINT('Ctrl Pts',(5.23167681249896,-4.95429886920134,334.873659727518));
#71770=CARTESIAN_POINT('Ctrl Pts',(5.23167681249894,-4.94521819965126,335.003514322247));
#71771=CARTESIAN_POINT('Ctrl Pts',(5.23167681249898,-4.93091661054929,335.133141271392));
#71772=CARTESIAN_POINT('Ctrl Pts',(5.23167681249902,-4.9112521298426,335.262270050933));
#71773=CARTESIAN_POINT('Ctrl Pts',(185.810302217248,3.4387199488324,339.81938086493));
#71774=CARTESIAN_POINT('Ctrl Pts',(185.763919407556,4.24130745050852,339.246723531428));
#71775=CARTESIAN_POINT('Ctrl Pts',(185.671163592151,5.54038606962475,337.695271231453));
#71776=CARTESIAN_POINT('Ctrl Pts',(185.485661765322,6.40062453626914,333.701383153881));
#71777=CARTESIAN_POINT('Ctrl Pts',(185.25379673676,3.50809689585563,328.942276555623));
#71778=CARTESIAN_POINT('Ctrl Pts',(184.975558702486,-3.20644657449587,328.772433974797));
#71779=CARTESIAN_POINT('Ctrl Pts',(184.697320668212,-6.96652177174833,334.325929885673));
#71780=CARTESIAN_POINT('Ctrl Pts',(184.419082633938,-4.33975135453482,340.493702333227));
#71781=CARTESIAN_POINT('Ctrl Pts',(184.140844599664,2.27283062225682,341.622249810224));
#71782=CARTESIAN_POINT('Ctrl Pts',(183.86260656539,6.79793088994909,336.672459105425));
#71783=CARTESIAN_POINT('Ctrl Pts',(183.584368531116,5.08559089065535,330.188511195752));
#71784=CARTESIAN_POINT('Ctrl Pts',(183.306130496843,-1.29420832154675,328.119659895712));
#71785=CARTESIAN_POINT('Ctrl Pts',(183.027892462568,-6.48607347215639,332.364972912782));
#71786=CARTESIAN_POINT('Ctrl Pts',(182.749654428295,-5.72590146837062,339.028317254472));
#71787=CARTESIAN_POINT('Ctrl Pts',(182.47141639402,0.288918215035514,341.994984166663));
#71788=CARTESIAN_POINT('Ctrl Pts',(182.193178359747,6.03856356499396,338.542430950412));
#71789=CARTESIAN_POINT('Ctrl Pts',(181.914940325473,6.24672857174619,331.839055121086));
#71790=CARTESIAN_POINT('Ctrl Pts',(181.636702291199,0.722352212805145,328.03642434573));
#71791=CARTESIAN_POINT('Ctrl Pts',(181.358464256925,-5.46491041299496,330.624168088303));
#71792=CARTESIAN_POINT('Ctrl Pts',(181.080226222651,-6.63710843185237,337.227546111849));
#71793=CARTESIAN_POINT('Ctrl Pts',(180.801988188377,-1.71852840848146,341.786739047181));
#71794=CARTESIAN_POINT('Ctrl Pts',(180.523750154103,4.77711892367299,340.1178411484));
#71795=CARTESIAN_POINT('Ctrl Pts',(180.245512119829,6.8888751779057,333.752376275502));
#71796=CARTESIAN_POINT('Ctrl Pts',(179.967274085555,2.67881212365101,328.531837116266));
#71797=CARTESIAN_POINT('Ctrl Pts',(179.689036051281,-3.98955715157227,329.24703565205));
#71798=CARTESIAN_POINT('Ctrl Pts',(179.410798017007,-6.99676878113797,335.241644610499));
#71799=CARTESIAN_POINT('Ctrl Pts',(179.132559982733,-3.58314893713384,341.014499900835));
#71800=CARTESIAN_POINT('Ctrl Pts',(178.854321948459,3.11867378061391,341.267937393193));
#71801=CARTESIAN_POINT('Ctrl Pts',(178.576083914186,6.95853561133084,335.769381261229));
#71802=CARTESIAN_POINT('Ctrl Pts',(178.297845879911,4.41265201410948,329.56477529828));
#71803=CARTESIAN_POINT('Ctrl Pts',(178.019607845638,-2.18265720304945,328.347994822222));
#71804=CARTESIAN_POINT('Ctrl Pts',(177.741369811363,-6.7749741224064,333.235661313365));
#71805=CARTESIAN_POINT('Ctrl Pts',(177.46313177709,-5.14999728730718,339.742435376173));
#71806=CARTESIAN_POINT('Ctrl Pts',(177.184893742816,1.20105604410647,341.897146492214));
#71807=CARTESIAN_POINT('Ctrl Pts',(176.906655708542,6.44991797161996,337.722448074217));
#71808=CARTESIAN_POINT('Ctrl Pts',(176.628417674268,5.77978537709548,331.0493992417));
#71809=CARTESIAN_POINT('Ctrl Pts',(176.350179639994,-0.194370948435958,
328.001758414345));
#71810=CARTESIAN_POINT('Ctrl Pts',(176.07194160572,-5.99015592353064,331.376300596248));
#71811=CARTESIAN_POINT('Ctrl Pts',(175.793703571446,-6.28886322214059,338.07625823527));
#71812=CARTESIAN_POINT('Ctrl Pts',(175.515465537172,-0.816373565270258,
341.953179097276));
#71813=CARTESIAN_POINT('Ctrl Pts',(175.237227502899,5.40529006279934,339.449270130471));
#71814=CARTESIAN_POINT('Ctrl Pts',(174.958989468624,6.666598782186,332.86233163605));
#71815=CARTESIAN_POINT('Ctrl Pts',(174.680751434351,1.81006819799868,328.237099847294));
#71816=CARTESIAN_POINT('Ctrl Pts',(174.402513400076,-4.70753525492994,329.818081708433));
#71817=CARTESIAN_POINT('Ctrl Pts',(174.124275365803,-6.90510308751545,336.154433500756));
#71818=CARTESIAN_POINT('Ctrl Pts',(173.846037331528,-2.76595973584276,341.431378708844));
#71819=CARTESIAN_POINT('Ctrl Pts',(173.567799297255,3.91146403991415,340.806342602822));
#71820=CARTESIAN_POINT('Ctrl Pts',(173.28956126298,6.99939499935638,334.852911591665));
#71821=CARTESIAN_POINT('Ctrl Pts',(173.011323228707,3.66408447879018,329.034461441817));
#71822=CARTESIAN_POINT('Ctrl Pts',(172.733085194433,-3.03370228616353,328.690497975607));
#71823=CARTESIAN_POINT('Ctrl Pts',(172.454847160159,-6.94750524047731,334.136671389087));
#71824=CARTESIAN_POINT('Ctrl Pts',(172.176609125885,-4.48568518061436,340.375108726091));
#71825=CARTESIAN_POINT('Ctrl Pts',(171.898371091611,2.09258196089365,341.680888121637));
#71826=CARTESIAN_POINT('Ctrl Pts',(171.620133057337,6.75051752334867,336.855715097703));
#71827=CARTESIAN_POINT('Ctrl Pts',(171.341895023063,5.21360279210196,330.327579718918));
#71828=CARTESIAN_POINT('Ctrl Pts',(171.063656988789,-1.1077582688056,328.087255467271));
#71829=CARTESIAN_POINT('Ctrl Pts',(170.785418954515,-6.41254591691553,332.190654841367));
#71830=CARTESIAN_POINT('Ctrl Pts',(170.507180920241,-5.83263482609468,338.872148801675));
#71831=CARTESIAN_POINT('Ctrl Pts',(170.228942885967,0.0997991550843282,
342.000228959508));
#71832=CARTESIAN_POINT('Ctrl Pts',(169.950704851693,5.94064892467557,338.704302324411));
#71833=CARTESIAN_POINT('Ctrl Pts',(169.672466817419,6.32985285992645,332.008992121615));
#71834=CARTESIAN_POINT('Ctrl Pts',(169.394228783146,0.910244254097873,328.058485701609));
#71835=CARTESIAN_POINT('Ctrl Pts',(169.115990748871,-5.34468206853313,330.478104496654));
#71836=CARTESIAN_POINT('Ctrl Pts',(168.837752714598,-6.69487254424932,337.047400052051));
#71837=CARTESIAN_POINT('Ctrl Pts',(168.559514680324,-1.90127730226469,341.737826799257));
#71838=CARTESIAN_POINT('Ctrl Pts',(168.28127664605,4.63709205720122,340.245049342945));
#71839=CARTESIAN_POINT('Ctrl Pts',(168.003038611776,6.92007047914019,333.938967521414));
#71840=CARTESIAN_POINT('Ctrl Pts',(167.724800577502,2.85260236244514,328.606579544669));
#71841=CARTESIAN_POINT('Ctrl Pts',(167.446562543228,-3.83265683792397,329.141339153049));
#71842=CARTESIAN_POINT('Ctrl Pts',(167.168324508954,-7.00074342805247,335.052505346985));
#71843=CARTESIAN_POINT('Ctrl Pts',(166.89008647468,-3.74435110506085,340.915488158969));
#71844=CARTESIAN_POINT('Ctrl Pts',(166.611848440406,2.9481769605134,341.349914799931));
#71845=CARTESIAN_POINT('Ctrl Pts',(166.333610406132,6.9352065444451,335.957118353584));
#71846=CARTESIAN_POINT('Ctrl Pts',(166.055372371858,4.55789944602034,329.685988521198));
#71847=CARTESIAN_POINT('Ctrl Pts',(165.777134337584,-2.00212469953175,328.291448588227));
#71848=CARTESIAN_POINT('Ctrl Pts',(165.498896303311,-6.72482855963568,333.053247267784));
#71849=CARTESIAN_POINT('Ctrl Pts',(165.220658269036,-5.27625650886877,339.601552195673));
#71850=CARTESIAN_POINT('Ctrl Pts',(164.942420234763,1.01425826266857,341.927080592391));
#71851=CARTESIAN_POINT('Ctrl Pts',(164.664182200489,6.3740031969824,337.895729373015));
#71852=CARTESIAN_POINT('Ctrl Pts',(164.385944166214,5.88441947755844,331.207010048917));
#71853=CARTESIAN_POINT('Ctrl Pts',(164.107706131941,-0.00520914253163273,
327.999061618489));
#71854=CARTESIAN_POINT('Ctrl Pts',(163.829468097667,-5.8900574094073,331.215771007091));
#71855=CARTESIAN_POINT('Ctrl Pts',(163.551230063393,-6.36968692877479,337.905211487359));
#71856=CARTESIAN_POINT('Ctrl Pts',(163.272992029119,-1.00394877003062,341.928582266528));
#71857=CARTESIAN_POINT('Ctrl Pts',(162.994753994845,5.28309835671109,339.593695365411));
#71858=CARTESIAN_POINT('Ctrl Pts',(162.716515960571,6.72192409990297,333.04324203029));
#71859=CARTESIAN_POINT('Ctrl Pts',(162.438277926297,1.99213931205097,328.288476602271));
#71860=CARTESIAN_POINT('Ctrl Pts',(162.160039892023,-4.56580231854216,329.692777134426));
#71861=CARTESIAN_POINT('Ctrl Pts',(161.881801857749,-6.9337745525409,335.967437755836));
#71862=CARTESIAN_POINT('Ctrl Pts',(161.603563823475,-2.93872422201748,341.354295028075));
#71863=CARTESIAN_POINT('Ctrl Pts',(161.325325789201,3.75314995155296,340.909909542289));
#71864=CARTESIAN_POINT('Ctrl Pts',(161.047087754927,7.00081381098573,335.042087299667));
#71865=CARTESIAN_POINT('Ctrl Pts',(160.768849720653,3.8239341679194,329.135642163348));
#71866=CARTESIAN_POINT('Ctrl Pts',(160.490611686379,-2.86211341987065,328.610831655945));
#71867=CARTESIAN_POINT('Ctrl Pts',(160.212373652106,-6.92164176697034,333.949266633911));
#71868=CARTESIAN_POINT('Ctrl Pts',(159.934135617832,-4.62928162778639,340.251944113139));
#71869=CARTESIAN_POINT('Ctrl Pts',(159.655897583558,1.91130193313229,341.734989998306));
#71870=CARTESIAN_POINT('Ctrl Pts',(159.377659549284,6.69791192078577,337.03743497032));
#71871=CARTESIAN_POINT('Ctrl Pts',(159.09942151501,5.33794699975203,330.47015594256));
#71872=CARTESIAN_POINT('Ctrl Pts',(158.821183480736,-0.920573094985571,
328.059847945927));
#71873=CARTESIAN_POINT('Ctrl Pts',(158.542945446462,-6.33429684809153,332.018415052839));
#71874=CARTESIAN_POINT('Ctrl Pts',(158.264707412188,-5.9351298777721,338.713138657639));
#71875=CARTESIAN_POINT('Ctrl Pts',(157.986469377914,-0.0893818209946288,
342.000369722162));
#71876=CARTESIAN_POINT('Ctrl Pts',(157.70823134364,5.83839061363612,338.863464817943));
#71877=CARTESIAN_POINT('Ctrl Pts',(157.429993309366,6.40835815663718,332.181115274946));
#71878=CARTESIAN_POINT('Ctrl Pts',(157.151755275092,1.09747000650366,328.08561463746));
#71879=CARTESIAN_POINT('Ctrl Pts',(156.873517240818,-5.22055016996747,330.335343391017));
#71880=CARTESIAN_POINT('Ctrl Pts',(156.595279206544,-6.74774851065374,336.865758664419));
#71881=CARTESIAN_POINT('Ctrl Pts',(156.31704117227,-2.08263763971794,341.683994750036));
#71882=CARTESIAN_POINT('Ctrl Pts',(156.038803137996,4.49367905350588,340.368427509146));
#71883=CARTESIAN_POINT('Ctrl Pts',(155.760565103723,6.94621280592146,334.126333580974));
#71884=CARTESIAN_POINT('Ctrl Pts',(155.482327069449,3.02430959227587,328.685990430246));
#71885=CARTESIAN_POINT('Ctrl Pts',(155.204089035175,-3.67295789546487,329.039920667053));
#71886=CARTESIAN_POINT('Ctrl Pts',(154.925851000901,-6.99960613530717,334.863327737078));
#71887=CARTESIAN_POINT('Ctrl Pts',(154.647612966627,-3.90281913879529,340.812156925509));
#71888=CARTESIAN_POINT('Ctrl Pts',(154.369374932353,2.77552737587297,341.427255490694));
#71889=CARTESIAN_POINT('Ctrl Pts',(154.091136898079,6.90681338441952,336.144156558206));
#71890=CARTESIAN_POINT('Ctrl Pts',(153.812898863805,4.69981869448273,329.811082039975));
#71891=CARTESIAN_POINT('Ctrl Pts',(153.534660829531,-1.82013024217066,328.239800945355));
#71892=CARTESIAN_POINT('Ctrl Pts',(153.256422795257,-6.6697725206623,332.872254742809));
#71893=CARTESIAN_POINT('Ctrl Pts',(152.978184760983,-5.39866300262332,339.457308957317));
#71894=CARTESIAN_POINT('Ctrl Pts',(152.699946726709,0.826719868787715,341.95195653147));
#71895=CARTESIAN_POINT('Ctrl Pts',(152.421708692435,6.29343411897757,338.0668962074));
#71896=CARTESIAN_POINT('Ctrl Pts',(152.143470658161,5.98475676911705,331.367390501116));
#71897=CARTESIAN_POINT('Ctrl Pts',(151.865232623887,0.183956467102918,328.001476914727));
#71898=CARTESIAN_POINT('Ctrl Pts',(151.586994589613,-5.78565796957856,331.058004665663));
#71899=CARTESIAN_POINT('Ctrl Pts',(151.30875655534,-6.44585948374944,337.732043351164));
#71900=CARTESIAN_POINT('Ctrl Pts',(151.030518521066,-1.19079089041349,341.898926178196));
#71901=CARTESIAN_POINT('Ctrl Pts',(150.752280486792,5.15704892701019,339.73476627948));
#71902=CARTESIAN_POINT('Ctrl Pts',(150.474042452518,6.77234106203401,333.225581251122));
#71903=CARTESIAN_POINT('Ctrl Pts',(150.195804418244,2.17275576401948,328.344754118231));
#71904=CARTESIAN_POINT('Ctrl Pts',(149.91756638397,-4.42073542881313,329.571347899771));
#71905=CARTESIAN_POINT('Ctrl Pts',(149.639328349696,-6.95738296857203,335.779735586917));
#71906=CARTESIAN_POINT('Ctrl Pts',(149.361090315422,-3.10934284887668,341.272571434828));
#71907=CARTESIAN_POINT('Ctrl Pts',(149.082852281148,3.59209530940757,341.009161059999));
#71908=CARTESIAN_POINT('Ctrl Pts',(148.804614246874,6.99712062148836,335.231232275482));
#71909=CARTESIAN_POINT('Ctrl Pts',(148.5263762126,3.98099161656035,329.241105044737));
#71910=CARTESIAN_POINT('Ctrl Pts',(148.248138178326,-2.68843463554514,328.535830713288));
#71911=CARTESIAN_POINT('Ctrl Pts',(147.969900144052,-6.89072410384103,333.762629125271));
#71912=CARTESIAN_POINT('Ctrl Pts',(147.691662109779,-4.76949776896307,340.124944525431));
#71913=CARTESIAN_POINT('Ctrl Pts',(147.413424075504,1.72862627082064,341.784173978658));
#71914=CARTESIAN_POINT('Ctrl Pts',(147.135186041231,6.64041549635417,337.217667105916));
#71915=CARTESIAN_POINT('Ctrl Pts',(146.856948006956,5.45839343325556,330.616039862787));
#71916=CARTESIAN_POINT('Ctrl Pts',(146.578709972683,-0.732715717786626,
328.037508130433));
#71917=CARTESIAN_POINT('Ctrl Pts',(146.300471938409,-6.25142246948224,331.84835242057));
#71918=CARTESIAN_POINT('Ctrl Pts',(146.022233904135,-6.03329109177857,338.551417176107));
#71919=CARTESIAN_POINT('Ctrl Pts',(145.743995869861,-0.278497530380219,
341.995398807964));
#71920=CARTESIAN_POINT('Ctrl Pts',(145.465757835587,5.73186910403123,339.019806205669));
#71921=CARTESIAN_POINT('Ctrl Pts',(145.187519801313,6.48218406392253,332.355296780674));
#71922=CARTESIAN_POINT('Ctrl Pts',(144.909281767039,1.28389438523206,328.1177924643));
#71923=CARTESIAN_POINT('Ctrl Pts',(144.631043732765,-5.09260622053579,330.19598842222));
#71924=CARTESIAN_POINT('Ctrl Pts',(144.352805698491,-6.79569726446257,336.682754897975));
#71925=CARTESIAN_POINT('Ctrl Pts',(144.074567664217,-2.26247723311923,341.62528204128));
#71926=CARTESIAN_POINT('Ctrl Pts',(143.796329629943,4.34698476094839,340.487885644304));
#71927=CARTESIAN_POINT('Ctrl Pts',(143.518091595669,6.96728300128357,334.314337592611));
#71928=CARTESIAN_POINT('Ctrl Pts',(143.239853561395,3.19380846826935,328.770011811818));
#71929=CARTESIAN_POINT('Ctrl Pts',(142.961615527121,-3.51057695553987,328.942854236844));
#71930=CARTESIAN_POINT('Ctrl Pts',(142.683377492847,-6.99335772328111,334.674249925394));
#71931=CARTESIAN_POINT('Ctrl Pts',(142.405139458574,-4.05843733015822,340.704581649346));
#71932=CARTESIAN_POINT('Ctrl Pts',(142.126901424299,2.60085109841411,341.499902993181));
#71933=CARTESIAN_POINT('Ctrl Pts',(141.848663390026,6.87337686247108,336.330359298584));
#71934=CARTESIAN_POINT('Ctrl Pts',(141.570425355752,4.83830613071455,329.939964511748));
#71935=CARTESIAN_POINT('Ctrl Pts',(141.292187321478,-1.63680672391732,328.193089606479));
#71936=CARTESIAN_POINT('Ctrl Pts',(141.013949287204,-6.60984620723789,332.692815899512));
#71937=CARTESIAN_POINT('Ctrl Pts',(140.73571125293,-5.51712738734636,339.309810987581));
#71938=CARTESIAN_POINT('Ctrl Pts',(140.457473218656,0.638577803246183,341.971756145054));
#71939=CARTESIAN_POINT('Ctrl Pts',(140.179235184382,6.20826956919261,338.235823591161));
#71940=CARTESIAN_POINT('Ctrl Pts',(139.900997150108,6.08072398539963,331.530423488339));
#71941=CARTESIAN_POINT('Ctrl Pts',(139.622759115834,0.372987751544304,328.009002539402));
#71942=CARTESIAN_POINT('Ctrl Pts',(139.34452108156,-5.67703383661305,330.903116773103));
#71943=CARTESIAN_POINT('Ctrl Pts',(139.066283047286,-6.51732526579266,337.556880274229));
#71944=CARTESIAN_POINT('Ctrl Pts',(138.788045013012,-1.37676349411775,341.864232487187));
#71945=CARTESIAN_POINT('Ctrl Pts',(138.509806978738,5.02723381511318,339.872379862558));
#71946=CARTESIAN_POINT('Ctrl Pts',(138.231568944464,6.81781285406428,333.40921615427));
#71947=CARTESIAN_POINT('Ctrl Pts',(137.953330910191,2.35178566759336,328.405891301276));
#71948=CARTESIAN_POINT('Ctrl Pts',(137.675092875917,-4.27244051372844,329.453882672218));
#71949=CARTESIAN_POINT('Ctrl Pts',(137.396854841643,-6.97591109672025,335.591464054306));
#71950=CARTESIAN_POINT('Ctrl Pts',(137.118616807369,-3.2776910305309,341.186267603754));
#71951=CARTESIAN_POINT('Ctrl Pts',(136.840378773095,3.42841771573635,341.104024682397));
#71952=CARTESIAN_POINT('Ctrl Pts',(136.562140738821,6.9883181276349,335.42020840526));
#71953=CARTESIAN_POINT('Ctrl Pts',(136.283902704547,4.13514214120938,329.350773076882));
#71954=CARTESIAN_POINT('Ctrl Pts',(136.005664670273,-2.51279275360601,328.465549913397));
#71955=CARTESIAN_POINT('Ctrl Pts',(135.727426635999,-6.85477482719744,333.576895146063));
#71956=CARTESIAN_POINT('Ctrl Pts',(135.449188601725,-4.90623121818037,339.994202698192));
#71957=CARTESIAN_POINT('Ctrl Pts',(135.170950567451,1.54468836390661,341.828404148504));
#71958=CARTESIAN_POINT('Ctrl Pts',(134.892712533177,6.57807023399944,337.396279898812));
#71959=CARTESIAN_POINT('Ctrl Pts',(134.614474498903,5.57485414250854,330.765124955016));
#71960=CARTESIAN_POINT('Ctrl Pts',(134.336236464629,-0.544323310850194,
328.020252333347));
#71961=CARTESIAN_POINT('Ctrl Pts',(134.057998430355,-6.1639832960406,331.680591124461));
#71962=CARTESIAN_POINT('Ctrl Pts',(133.779760396081,-6.12704679069886,338.387102446261));
#71963=CARTESIAN_POINT('Ctrl Pts',(133.501522361807,-0.467409880595166,
341.985319846679));
#71964=CARTESIAN_POINT('Ctrl Pts',(133.223284327534,5.62116217797218,339.173212326951));
#71965=CARTESIAN_POINT('Ctrl Pts',(132.94504629326,6.55127667403222,332.531409451293));
#71966=CARTESIAN_POINT('Ctrl Pts',(132.666808258985,1.46938126301808,328.154995685847));
#71967=CARTESIAN_POINT('Ctrl Pts',(132.388570224712,-4.96094364503585,330.060141347401));
#71968=CARTESIAN_POINT('Ctrl Pts',(132.110332190438,-6.83868379344855,336.49852238225));
#71969=CARTESIAN_POINT('Ctrl Pts',(131.832094156164,-2.44066476342085,341.561731545064));
#71970=CARTESIAN_POINT('Ctrl Pts',(131.55385612189,4.19711629584524,340.60333651997));
#71971=CARTESIAN_POINT('Ctrl Pts',(131.275618087616,6.98326567974919,334.502842275613));
#71972=CARTESIAN_POINT('Ctrl Pts',(130.997380053342,3.36097522217991,328.858582336889));
#71973=CARTESIAN_POINT('Ctrl Pts',(130.719142019068,-3.34563258887094,328.850210740427));
#71974=CARTESIAN_POINT('Ctrl Pts',(130.440903984794,-6.98200275457099,334.485409976734));
#71975=CARTESIAN_POINT('Ctrl Pts',(130.16266595052,-4.21109204659298,340.592840882057));
#71976=CARTESIAN_POINT('Ctrl Pts',(129.884427916246,2.42427567692669,341.567804260112));
#71977=CARTESIAN_POINT('Ctrl Pts',(129.606189881972,6.83492139398107,336.515590609294));
#71978=CARTESIAN_POINT('Ctrl Pts',(129.327951847698,4.97326063105343,330.072541826409));
#71979=CARTESIAN_POINT('Ctrl Pts',(129.049713813425,-1.45228800778535,328.151348680264));
#71980=CARTESIAN_POINT('Ctrl Pts',(128.771475779151,-6.54509337761538,332.515061764314));
#71981=CARTESIAN_POINT('Ctrl Pts',(128.493237744877,-5.63156316022767,339.159165989624));
#71982=CARTESIAN_POINT('Ctrl Pts',(128.214999710603,0.449969447564982,341.986464975446));
#71983=CARTESIAN_POINT('Ctrl Pts',(127.936761676329,6.11857173486536,338.402388173355));
#71984=CARTESIAN_POINT('Ctrl Pts',(127.658523642055,6.17225105105066,331.695989963744));
#71985=CARTESIAN_POINT('Ctrl Pts',(127.380285607781,0.561746679963059,328.021632997296));
#71986=CARTESIAN_POINT('Ctrl Pts',(127.102047573507,-5.5642643279593,330.751220428702));
#71987=CARTESIAN_POINT('Ctrl Pts',(126.823809539233,-6.58403209052025,337.379850160804));
#71988=CARTESIAN_POINT('Ctrl Pts',(126.545571504959,-1.56173078376513,341.824526526868));
#71989=CARTESIAN_POINT('Ctrl Pts',(126.267333470685,4.89374781214267,340.006435629071));
#71990=CARTESIAN_POINT('Ctrl Pts',(125.989095436411,6.85830627244645,333.594012649345));
#71991=CARTESIAN_POINT('Ctrl Pts',(125.710857402137,2.52909829496077,328.471843508975));
#71992=CARTESIAN_POINT('Ctrl Pts',(125.432619367863,-4.12102585838077,329.340467224988));
#71993=CARTESIAN_POINT('Ctrl Pts',(125.154381333589,-6.98934540772823,335.402760634062));
#71994=CARTESIAN_POINT('Ctrl Pts',(124.876143299315,-3.44364583897262,341.095446553995));
#71995=CARTESIAN_POINT('Ctrl Pts',(124.597905265041,3.2622366880789,341.194431139971));
#71996=CARTESIAN_POINT('Ctrl Pts',(124.319667230768,6.97441275701501,335.608877698449));
#71997=CARTESIAN_POINT('Ctrl Pts',(124.041429196494,4.28627318100201,329.464566180081));
#71998=CARTESIAN_POINT('Ctrl Pts',(123.76319116222,-2.33531602792795,328.400040575383));
#71999=CARTESIAN_POINT('Ctrl Pts',(123.484953127946,-6.8138201872366,333.392200319416));
#72000=CARTESIAN_POINT('Ctrl Pts',(123.206715093672,-5.03938213253937,339.859814099235));
#72001=CARTESIAN_POINT('Ctrl Pts',(122.928477059398,1.3596225240309,341.867648210926));
#72002=CARTESIAN_POINT('Ctrl Pts',(122.650239025124,6.51092165829356,337.573142925771));
#72003=CARTESIAN_POINT('Ctrl Pts',(122.37200099085,5.68724408778636,330.917302357164));
#72004=CARTESIAN_POINT('Ctrl Pts',(122.093762956576,-0.355533438497236,
328.008093154869));
#72005=CARTESIAN_POINT('Ctrl Pts',(121.815524922302,-6.07204317593688,331.515253663975));
#72006=CARTESIAN_POINT('Ctrl Pts',(121.537286888028,-6.21632851402961,338.220314450879));
#72007=CARTESIAN_POINT('Ctrl Pts',(121.259048853754,-0.655980927655841,
341.970140197976));
#72008=CARTESIAN_POINT('Ctrl Pts',(120.98081081948,5.50635067376508,339.32357116449));
#72009=CARTESIAN_POINT('Ctrl Pts',(120.702572785207,6.6155855354745,332.709324689158));
#72010=CARTESIAN_POINT('Ctrl Pts',(120.424334750932,1.65379519716147,328.197197136273));
#72011=CARTESIAN_POINT('Ctrl Pts',(120.146096716659,-4.82565858360948,329.927901362226));
#72012=CARTESIAN_POINT('Ctrl Pts',(119.867858682384,-6.87667670880607,336.31319564401));
#72013=CARTESIAN_POINT('Ctrl Pts',(119.589620648111,-2.61707011791319,341.493389666023));
#72014=CARTESIAN_POINT('Ctrl Pts',(119.311382613837,4.044183092297,340.714695833801));
#72015=CARTESIAN_POINT('Ctrl Pts',(119.033144579563,6.99414917075083,334.691709983673));
#72016=CARTESIAN_POINT('Ctrl Pts',(118.754906545289,3.52568778867917,328.951637331174));
#72017=CARTESIAN_POINT('Ctrl Pts',(118.476668511015,-3.17824523799691,328.762057826172));
#72018=CARTESIAN_POINT('Ctrl Pts',(118.198430476741,-6.96554952058604,334.296945782214));
#72019=CARTESIAN_POINT('Ctrl Pts',(117.920192442467,-4.36067181947576,340.477016216857));
#72020=CARTESIAN_POINT('Ctrl Pts',(117.641954408193,2.24593004695689,341.630909709916));
#72021=CARTESIAN_POINT('Ctrl Pts',(117.363716373919,6.79147505917034,336.699715234253));
#72022=CARTESIAN_POINT('Ctrl Pts',(117.085478339645,5.10458365159074,330.208717175871));
#72023=CARTESIAN_POINT('Ctrl Pts',(116.807240305371,-1.26670882952249,328.114608645974));
#72024=CARTESIAN_POINT('Ctrl Pts',(116.529002271097,-6.4755613143746,332.339122133457));
#72025=CARTESIAN_POINT('Ctrl Pts',(116.250764236823,-5.74188676015347,339.005483964574));
#72026=CARTESIAN_POINT('Ctrl Pts',(115.97252620255,0.26103252375085,341.996072282246));
#72027=CARTESIAN_POINT('Ctrl Pts',(115.694288168275,6.02440611344274,338.566468328361));
#72028=CARTESIAN_POINT('Ctrl Pts',(115.416050134002,6.25927113291671,331.863969030523));
#72029=CARTESIAN_POINT('Ctrl Pts',(115.137812099727,0.7500954204035,328.039359065635));
#72030=CARTESIAN_POINT('Ctrl Pts',(114.859574065454,-5.44743178802376,330.602426547321));
#72031=CARTESIAN_POINT('Ctrl Pts',(114.58133603118,-6.64593124854297,337.201082278453));
#72032=CARTESIAN_POINT('Ctrl Pts',(114.303097996906,-1.74555769605902,341.77983729057));
#72033=CARTESIAN_POINT('Ctrl Pts',(114.024859962632,4.75668838970893,340.136835691367));
#72034=CARTESIAN_POINT('Ctrl Pts',(113.746621928358,6.89379174884668,333.779835797765));
#72035=CARTESIAN_POINT('Ctrl Pts',(113.468383894084,2.70456417226724,328.542562582962));
#72036=CARTESIAN_POINT('Ctrl Pts',(113.19014585981,-3.9666020259001,329.231184374154));
#72037=CARTESIAN_POINT('Ctrl Pts',(112.911907825536,-6.99767609184886,335.213763117606));
#72038=CARTESIAN_POINT('Ctrl Pts',(112.633669791262,-3.60708609383773,341.00017460317));
#72039=CARTESIAN_POINT('Ctrl Pts',(112.355431756988,3.09367357198481,341.280314417837));
#72040=CARTESIAN_POINT('Ctrl Pts',(112.077193722714,6.95541466334396,335.797102388544));
#72041=CARTESIAN_POINT('Ctrl Pts',(111.79895568844,4.43427437990451,329.582401262496));
#72042=CARTESIAN_POINT('Ctrl Pts',(111.520717654166,-2.15613405219075,328.33935053423));
#72043=CARTESIAN_POINT('Ctrl Pts',(111.242479619892,-6.767890089077,333.208679509676));
#72044=CARTESIAN_POINT('Ctrl Pts',(110.964241585619,-5.16885328511126,339.721876859245));
#72045=CARTESIAN_POINT('Ctrl Pts',(110.686003551344,1.17356388645166,341.901877509873));
#72046=CARTESIAN_POINT('Ctrl Pts',(110.407765517071,6.43901880119245,337.748127041236));
#72047=CARTESIAN_POINT('Ctrl Pts',(110.129527482797,5.79548120184066,331.072460949145));
#72048=CARTESIAN_POINT('Ctrl Pts',(109.851289448523,-0.166483955278002,
328.001039473642));
#72049=CARTESIAN_POINT('Ctrl Pts',(109.573051414249,-5.97566924393718,331.35246076869));
#72050=CARTESIAN_POINT('Ctrl Pts',(109.294813379975,-6.30107106816867,338.051174978721));
#72051=CARTESIAN_POINT('Ctrl Pts',(109.016575345701,-0.844072976798288,
341.949870946048));
#72052=CARTESIAN_POINT('Ctrl Pts',(108.738337311427,5.38751842688317,339.470772926115));
#72053=CARTESIAN_POINT('Ctrl Pts',(108.460099277153,6.67506368985558,332.888912580385));
#72054=CARTESIAN_POINT('Ctrl Pts',(108.181861242879,1.83700152842608,328.244366000038));
#72055=CARTESIAN_POINT('Ctrl Pts',(107.903623208605,-4.6868498215419,329.799365028462));
#72056=CARTESIAN_POINT('Ctrl Pts',(107.625385174331,-6.90964826807086,336.126910009019));
#72057=CARTESIAN_POINT('Ctrl Pts',(107.347147140057,-2.79156448523252,341.420306307465));
#72058=CARTESIAN_POINT('Ctrl Pts',(107.068909105783,3.88829682227926,340.821882271116));
#72059=CARTESIAN_POINT('Ctrl Pts',(106.790671071509,6.99992552715261,334.880802805406));
#72060=CARTESIAN_POINT('Ctrl Pts',(106.512433037235,3.68782589448949,329.049108845827));
#72061=CARTESIAN_POINT('Ctrl Pts',(106.234195002962,-3.00853712932565,328.678459863423));
#72062=CARTESIAN_POINT('Ctrl Pts',(105.955956968688,-6.94401003549388,334.108994958577));
#72063=CARTESIAN_POINT('Ctrl Pts',(105.677718934414,-4.50706742550949,340.357192229032));
#72064=CARTESIAN_POINT('Ctrl Pts',(105.39948090014,2.0659444366588,341.689173262932));
#72065=CARTESIAN_POINT('Ctrl Pts',(105.121242865866,6.74306958259522,336.882598725476));
#72066=CARTESIAN_POINT('Ctrl Pts',(104.843004831592,5.2321793001279,330.348391124762));
#72067=CARTESIAN_POINT('Ctrl Pts',(104.564766797318,-1.08020469922692,328.082896331221));
#72068=CARTESIAN_POINT('Ctrl Pts',(104.286528763044,-6.40130078989642,332.165125478235));
#72069=CARTESIAN_POINT('Ctrl Pts',(104.00829072877,-5.84801762872275,338.848877131195));
#72070=CARTESIAN_POINT('Ctrl Pts',(103.730052694496,0.0719049937310667,
342.00057105019));
#72071=CARTESIAN_POINT('Ctrl Pts',(103.451814660222,5.92584146475386,338.727944244686));
#72072=CARTESIAN_POINT('Ctrl Pts',(103.173576625948,6.34172068884867,332.0342380302));
#72073=CARTESIAN_POINT('Ctrl Pts',(102.895338591674,0.937896440430998,328.062167800825));
#72074=CARTESIAN_POINT('Ctrl Pts',(102.6171005574,-5.32662152804144,330.456843778397));
#72075=CARTESIAN_POINT('Ctrl Pts',(102.338862523126,-6.70297754103513,337.020707163659));
#72076=CARTESIAN_POINT('Ctrl Pts',(102.060624488853,-1.9281100004072,341.730197410419));
#72077=CARTESIAN_POINT('Ctrl Pts',(101.782386454578,4.61615562873744,340.263484831189));
#72078=CARTESIAN_POINT('Ctrl Pts',(101.504148420305,6.92424337173514,333.966549911286));
#72079=CARTESIAN_POINT('Ctrl Pts',(101.225910386031,2.87805517415613,328.617996884097));
#72080=CARTESIAN_POINT('Ctrl Pts',(100.947672351757,-3.80928177672123,329.126113918161));
#72081=CARTESIAN_POINT('Ctrl Pts',(100.669434317483,-7.00089706600837,335.024609511113));
#72082=CARTESIAN_POINT('Ctrl Pts',(100.391196283209,-3.76789245089095,340.900521318951));
#72083=CARTESIAN_POINT('Ctrl Pts',(100.112958248935,2.92285145240769,341.361611803942));
#72084=CARTESIAN_POINT('Ctrl Pts',(99.8347202146609,6.93133771904842,335.98474503369));
#72085=CARTESIAN_POINT('Ctrl Pts',(99.5564821803873,4.57903766729572,329.704192280836));
#72086=CARTESIAN_POINT('Ctrl Pts',(99.2782441461129,-1.97537766524897,328.283524105863));
#72087=CARTESIAN_POINT('Ctrl Pts',(99.0000061118395,-6.71701807092136,333.026466723919));
#72088=CARTESIAN_POINT('Ctrl Pts',(98.7217680775651,-5.29455013593342,339.580491700131));
#72089=CARTESIAN_POINT('Ctrl Pts',(98.4435300432915,0.986648311368706,341.931067051079));
#72090=CARTESIAN_POINT('Ctrl Pts',(98.1652920090174,6.36241416623298,337.921104471635));
#72091=CARTESIAN_POINT('Ctrl Pts',(97.8870539747435,5.8994864498244,331.230487434001));
#72092=CARTESIAN_POINT('Ctrl Pts',(97.6088159404696,0.0226870946892429,
327.999096440272));
#72093=CARTESIAN_POINT('Ctrl Pts',(97.3305779061955,-5.87493187238127,331.192331310138));
#72094=CARTESIAN_POINT('Ctrl Pts',(97.0523398719218,-6.38121257401978,337.879807535592));
#72095=CARTESIAN_POINT('Ctrl Pts',(96.7741018376478,-1.03154868302355,341.924526891523));
#72096=CARTESIAN_POINT('Ctrl Pts',(96.4958638033737,5.2647522087498,339.614710124953));
#72097=CARTESIAN_POINT('Ctrl Pts',(96.2176257691,6.72966770616867,333.070041989723));
#72098=CARTESIAN_POINT('Ctrl Pts',(95.9393877348259,2.01886647936908,328.296467834391));
#72099=CARTESIAN_POINT('Ctrl Pts',(95.661149700552,-4.54461871712713,329.674626203466));
#72100=CARTESIAN_POINT('Ctrl Pts',(95.3829116662781,-6.93757439537808,335.939801503232));
#72101=CARTESIAN_POINT('Ctrl Pts',(95.104673632004,-2.96402044942079,341.342534834931));
#72102=CARTESIAN_POINT('Ctrl Pts',(94.8264355977303,3.72957131409984,340.924817564273));
#72103=CARTESIAN_POINT('Ctrl Pts',(94.5481975634562,7.00059053105341,335.069982665048));
#72104=CARTESIAN_POINT('Ctrl Pts',(94.2699595291823,3.84727114620612,329.15092570705));
#72105=CARTESIAN_POINT('Ctrl Pts',(93.9917214949084,-2.83663218388548,328.599477895498));
#72106=CARTESIAN_POINT('Ctrl Pts',(93.7134834606343,-6.91740002744779,333.921694747696));
#72107=CARTESIAN_POINT('Ctrl Pts',(93.4352454263607,-4.6501719664783,340.233456414174));
#72108=CARTESIAN_POINT('Ctrl Pts',(93.1570073920864,1.88445027170261,341.742552375055));
#72109=CARTESIAN_POINT('Ctrl Pts',(92.8787693578127,6.68974030998245,337.064107541259));
#72110=CARTESIAN_POINT('Ctrl Pts',(92.6005313235387,5.35595440619652,330.491461683025));
#72111=CARTESIAN_POINT('Ctrl Pts',(92.3222932892648,-0.892911802398389,
328.056234892364));
#72112=CARTESIAN_POINT('Ctrl Pts',(92.0440552549908,-6.32236602928883,331.993198851175));
#72113=CARTESIAN_POINT('Ctrl Pts',(91.7658172207168,-5.94987826907084,338.68945984395));
#72114=CARTESIAN_POINT('Ctrl Pts',(91.487579186443,-0.117275041385807,341.99995799427));
#72115=CARTESIAN_POINT('Ctrl Pts',(91.2093411521688,5.82294976080219,338.88669801246));
#72116=CARTESIAN_POINT('Ctrl Pts',(90.9311031178951,6.41953951409962,332.206672632183));
#72117=CARTESIAN_POINT('Ctrl Pts',(90.6528650836211,1.12501260755572,328.090042547907));
#72118=CARTESIAN_POINT('Ctrl Pts',(90.3746270493473,-5.20192176378319,330.314578426613));
#72119=CARTESIAN_POINT('Ctrl Pts',(90.0963890150731,-6.75512931273765,336.838856526506));
#72120=CARTESIAN_POINT('Ctrl Pts',(89.8181509807993,-2.10925439693799,341.675643133503));
#72121=CARTESIAN_POINT('Ctrl Pts',(89.5399129465253,4.47225214638779,340.386290569215));
#72122=CARTESIAN_POINT('Ctrl Pts',(89.2616749122515,6.94963890530698,334.154018651077));
#72123=CARTESIAN_POINT('Ctrl Pts',(88.9834368779774,3.04944461732804,328.698091330182));
#72124=CARTESIAN_POINT('Ctrl Pts',(88.7051988437036,-3.64917998624406,329.025332579559));
#72125=CARTESIAN_POINT('Ctrl Pts',(88.4269608094296,-6.9990059782483,334.835437934729));
#72126=CARTESIAN_POINT('Ctrl Pts',(88.1487227751557,-3.92594748917296,340.796559468266));
#72127=CARTESIAN_POINT('Ctrl Pts',(87.8704847408817,2.74989506382644,341.438263934852));
#72128=CARTESIAN_POINT('Ctrl Pts',(87.5922467066078,6.90219950513693,336.171668617046));
#72129=CARTESIAN_POINT('Ctrl Pts',(87.3140086723338,4.72045733688097,329.829850303176));
#72130=CARTESIAN_POINT('Ctrl Pts',(87.03577063806,-1.79317885559459,328.232602054798));
#72131=CARTESIAN_POINT('Ctrl Pts',(86.7575326037859,-6.6612412795675,332.845695014101));
#72132=CARTESIAN_POINT('Ctrl Pts',(86.4792945695121,-5.41638090104145,339.435761861475));
#72133=CARTESIAN_POINT('Ctrl Pts',(86.201056535238,0.799012284719287,341.95519552031));
#72134=CARTESIAN_POINT('Ctrl Pts',(85.9228185009643,6.28116369019514,338.091948908675));
#72135=CARTESIAN_POINT('Ctrl Pts',(85.6445804666901,5.99918388700299,331.391266420639));
#72136=CARTESIAN_POINT('Ctrl Pts',(85.3663424324163,0.211841578517241,328.002265473563));
#72137=CARTESIAN_POINT('Ctrl Pts',(85.0881043981423,-5.76990461979722,331.034982215006));
#72138=CARTESIAN_POINT('Ctrl Pts',(84.8098663638684,-6.45669451217634,337.70633725417));
#72139=CARTESIAN_POINT('Ctrl Pts',(84.5316283295946,-1.21827115138629,341.894126540657));
#72140=CARTESIAN_POINT('Ctrl Pts',(84.2533902953204,5.13814166337825,339.755277657923));
#72141=CARTESIAN_POINT('Ctrl Pts',(83.9751522610467,6.77935771250735,333.252580656297));
#72142=CARTESIAN_POINT('Ctrl Pts',(83.6969142267727,2.19925725202426,328.35346459452));
#72143=CARTESIAN_POINT('Ctrl Pts',(83.4186761924987,-4.39906912765766,329.553775971651));
#72144=CARTESIAN_POINT('Ctrl Pts',(83.1404381582248,-6.96043469904204,335.752006753462));
#72145=CARTESIAN_POINT('Ctrl Pts',(82.8622001239508,-3.13431208296329,341.260132037224));
#72146=CARTESIAN_POINT('Ctrl Pts',(82.583962089677,3.56812246928036,341.023426549822));
#72147=CARTESIAN_POINT('Ctrl Pts',(82.3057240554029,6.99614369686675,335.259111423279));
#72148=CARTESIAN_POINT('Ctrl Pts',(82.0274860211291,4.00390711675021,329.257013568072));
#72149=CARTESIAN_POINT('Ctrl Pts',(81.749247986855,-2.66265592683582,328.525169595103));
#72150=CARTESIAN_POINT('Ctrl Pts',(81.4710099525813,-6.88573892710168,333.73518191637));
#72151=CARTESIAN_POINT('Ctrl Pts',(81.1927719183071,-4.78988094730629,340.105899124299));
#72152=CARTESIAN_POINT('Ctrl Pts',(80.9145338840334,1.70158007930518,341.791008068806));
#72153=CARTESIAN_POINT('Ctrl Pts',(80.6362958497593,6.63152618241909,337.244109143685));
#72154=CARTESIAN_POINT('Ctrl Pts',(80.3580578154855,5.475818589093,330.637824380401));
#72155=CARTESIAN_POINT('Ctrl Pts',(80.0798197812114,-0.704966900493841,
328.034643797615));
#72156=CARTESIAN_POINT('Ctrl Pts',(79.8015817469376,-6.23881467079188,331.82346779327));
#72157=CARTESIAN_POINT('Ctrl Pts',(79.5233437126635,-6.04739430245781,338.527348509502));
#72158=CARTESIAN_POINT('Ctrl Pts',(79.2451056783897,-0.306369442151794,
341.994233562142));
#72159=CARTESIAN_POINT('Ctrl Pts',(78.9668676441157,5.71580613321137,339.042613709523));
#72160=CARTESIAN_POINT('Ctrl Pts',(78.6886296098418,6.4926707852867,332.381146924556));
#72161=CARTESIAN_POINT('Ctrl Pts',(78.4103915755678,1.31130728936813,328.122962952715));
#72162=CARTESIAN_POINT('Ctrl Pts',(78.1321535412939,-5.07342355113972,330.175734374268));
#72163=CARTESIAN_POINT('Ctrl Pts',(77.8539155070199,-6.8023484823755,336.655663154511));
#72164=CARTESIAN_POINT('Ctrl Pts',(77.575677472746,-2.28885861383431,341.616214295407));
#72165=CARTESIAN_POINT('Ctrl Pts',(77.2974394384722,4.32508302112474,340.505163232572));
#72166=CARTESIAN_POINT('Ctrl Pts',(77.0192014041981,6.96995980571845,334.342105127281));
#72167=CARTESIAN_POINT('Ctrl Pts',(76.7409633699243,3.21860735304273,328.782787436172));
#72168=CARTESIAN_POINT('Ctrl Pts',(76.4627253356503,-3.48641356095375,328.928913948982));
#72169=CARTESIAN_POINT('Ctrl Pts',(76.1844873013764,-6.99200420944275,334.646386521726));
#72170=CARTESIAN_POINT('Ctrl Pts',(75.9062492671024,-4.08113579673913,340.688364964158));
#72171=CARTESIAN_POINT('Ctrl Pts',(75.6280112328284,2.5749306991664,341.51021483911));
#72172=CARTESIAN_POINT('Ctrl Pts',(75.3497731985546,6.86802129836172,336.357736646825));
#72173=CARTESIAN_POINT('Ctrl Pts',(75.0715351642804,4.85843012387871,329.959283573908));
#72174=CARTESIAN_POINT('Ctrl Pts',(74.7932971300068,-1.60967066497673,328.186621564364));
#72175=CARTESIAN_POINT('Ctrl Pts',(74.5150590957326,-6.60060044328308,332.666496379903));
#72176=CARTESIAN_POINT('Ctrl Pts',(74.2368210614589,-5.5342566194914,339.287793025146));
#72177=CARTESIAN_POINT('Ctrl Pts',(73.9585830271847,0.61079281851374,341.974245298937));
#72178=CARTESIAN_POINT('Ctrl Pts',(73.680344992911,6.19532670225604,338.260535601584));
#72179=CARTESIAN_POINT('Ctrl Pts',(73.4021069586369,6.09450071421021,331.554680508085));
#72180=CARTESIAN_POINT('Ctrl Pts',(73.1238689243631,0.400841375416753,328.010544259484));
#72181=CARTESIAN_POINT('Ctrl Pts',(72.845630890089,-5.66066417718765,330.880528379757));
#72182=CARTESIAN_POINT('Ctrl Pts',(72.5673928558152,-6.52746176565324,337.530890802626));
#72183=CARTESIAN_POINT('Ctrl Pts',(72.2891548215411,-1.40410403695659,341.858692091811));
#72184=CARTESIAN_POINT('Ctrl Pts',(72.0109167872673,5.00777924191351,339.892372882472));
#72185=CARTESIAN_POINT('Ctrl Pts',(71.7326787529933,6.82409742518003,333.436395290192));
#72186=CARTESIAN_POINT('Ctrl Pts',(71.4544407187194,2.37804212487173,328.415314661337));
#72187=CARTESIAN_POINT('Ctrl Pts',(71.1762026844454,-4.25030733358714,329.436902577975));
#72188=CARTESIAN_POINT('Ctrl Pts',(70.8979646501716,-6.9782124864465,335.563662887623));
#72189=CARTESIAN_POINT('Ctrl Pts',(70.6197266158975,-3.30231503874137,341.17315808495));
#72190=CARTESIAN_POINT('Ctrl Pts',(70.3414885816236,3.40406817792663,341.117637223382));
#72191=CARTESIAN_POINT('Ctrl Pts',(70.0632505473498,6.98658827167532,335.448050978093));
#72192=CARTESIAN_POINT('Ctrl Pts',(69.7850125130757,4.15761943038146,329.367294963431));
#72193=CARTESIAN_POINT('Ctrl Pts',(69.5067744788019,-2.48673539581103,328.455589222237));
#72194=CARTESIAN_POINT('Ctrl Pts',(69.2285364445278,-6.84904985342219,333.549592656451));
#72195=CARTESIAN_POINT('Ctrl Pts',(68.950298410254,-4.92609235235802,339.974613501864));
#72196=CARTESIAN_POINT('Ctrl Pts',(68.67206037598,1.51746739146117,341.83450496179));
#72197=CARTESIAN_POINT('Ctrl Pts',(68.3938223417061,6.56846970791843,337.422472095411));
#72198=CARTESIAN_POINT('Ctrl Pts',(68.1155843074321,5.59168432387292,330.787372342702));
#72199=CARTESIAN_POINT('Ctrl Pts',(67.8373462731582,-0.516507231065439,
328.018138812814));
#72200=CARTESIAN_POINT('Ctrl Pts',(67.5591082388843,-6.15070772368928,331.656056242305));
#72201=CARTESIAN_POINT('Ctrl Pts',(67.2808702046103,-6.14049452258065,338.362661501703));
#72202=CARTESIAN_POINT('Ctrl Pts',(67.0026321703365,-0.495240131650347,
341.983401933791));
#72203=CARTESIAN_POINT('Ctrl Pts',(66.7243941360623,5.60448881836311,339.195577486083));
#72204=CARTESIAN_POINT('Ctrl Pts',(66.4461561017886,6.56106110188412,332.557533506018));
#72205=CARTESIAN_POINT('Ctrl Pts',(66.1679180675145,1.49664445330917,328.160904976734));
#72206=CARTESIAN_POINT('Ctrl Pts',(65.8896800332407,-4.94122071963166,330.040413005424));
#72207=CARTESIAN_POINT('Ctrl Pts',(65.6114419989667,-6.84460057046481,336.471260815653));
#72208=CARTESIAN_POINT('Ctrl Pts',(65.3332039646927,-2.4667915039212,341.55195429113));
#72209=CARTESIAN_POINT('Ctrl Pts',(65.0549659304188,4.17475571598797,340.620016020326));
#72210=CARTESIAN_POINT('Ctrl Pts',(64.7767278961449,6.98519123462835,334.530671998967));
#72211=CARTESIAN_POINT('Ctrl Pts',(64.4984898618709,3.38541985850391,328.872023356889));
#72212=CARTESIAN_POINT('Ctrl Pts',(64.220251827597,-3.32110135305436,328.836928431404));
#72213=CARTESIAN_POINT('Ctrl Pts',(63.942013793323,-6.97989687229026,334.457593317636));
#72214=CARTESIAN_POINT('Ctrl Pts',(63.6637757590492,-4.23334405493435,340.576016810361));
#72215=CARTESIAN_POINT('Ctrl Pts',(63.3855377247751,2.39808611757899,341.577411978093));
#72216=CARTESIAN_POINT('Ctrl Pts',(63.1072996905013,6.82882805568316,336.54281325597));
#72217=CARTESIAN_POINT('Ctrl Pts',(62.8290616562273,4.99285528042379,330.09239758073));
#72218=CARTESIAN_POINT('Ctrl Pts',(62.5508236219534,-1.42498709125737,328.145616209561));
#72219=CARTESIAN_POINT('Ctrl Pts',(62.2725855876794,-6.53513984206652,332.489001672339));
#72220=CARTESIAN_POINT('Ctrl Pts',(61.9943475534055,-5.6480912183174,339.136693238137));
#72221=CARTESIAN_POINT('Ctrl Pts',(61.7161095191316,0.422127350791677,341.988202476788));
#72222=CARTESIAN_POINT('Ctrl Pts',(61.4378714848576,6.10496588066887,338.426741448192));
#72223=CARTESIAN_POINT('Ctrl Pts',(61.1596334505837,6.1853673310049,331.720610371209));
#72224=CARTESIAN_POINT('Ctrl Pts',(60.8813954163097,0.589548477549911,328.023926752858));
#72225=CARTESIAN_POINT('Ctrl Pts',(60.6031573820358,-5.54729031203137,330.729082586735));
#72226=CARTESIAN_POINT('Ctrl Pts',(60.3249193477619,-6.59346266013225,337.35359629213));
#72227=CARTESIAN_POINT('Ctrl Pts',(60.046681313488,-1.58891164437911,341.81824941926));
#72228=CARTESIAN_POINT('Ctrl Pts',(59.768443279214,4.87376013512332,340.025895691533));
#72229=CARTESIAN_POINT('Ctrl Pts',(59.49020524494,6.86385417520475,333.621351669785));
#72230=CARTESIAN_POINT('Ctrl Pts',(59.2119672106661,2.55509054902234,328.48197287186));
#72231=CARTESIAN_POINT('Ctrl Pts',(58.9337291763922,-4.09844196092319,329.324091363506));
#72232=CARTESIAN_POINT('Ctrl Pts',(58.6554911421182,-6.99089477623369,335.374907434589));
#72233=CARTESIAN_POINT('Ctrl Pts',(58.3772531078443,-3.46790664083229,341.081676486574));
#72234=CARTESIAN_POINT('Ctrl Pts',(58.0990150735703,3.23752823264279,341.207380792228));
#72235=CARTESIAN_POINT('Ctrl Pts',(57.8207770392965,6.97193123285997,335.636663365645));
#72236=CARTESIAN_POINT('Ctrl Pts',(57.5425390050225,4.30829584621786,329.481689365544));
#72237=CARTESIAN_POINT('Ctrl Pts',(57.2643009707486,-2.30899904815591,328.390787584553));
#72238=CARTESIAN_POINT('Ctrl Pts',(56.9860629364746,-6.80735959680711,333.365062485402));
#72239=CARTESIAN_POINT('Ctrl Pts',(56.7078249022006,-5.05870671993135,339.839695411759));
#72240=CARTESIAN_POINT('Ctrl Pts',(56.4295868679267,1.3322466474366,341.873011292532));
#72241=CARTESIAN_POINT('Ctrl Pts',(56.1513488336528,6.50061693038027,337.599066155629));
#72242=CARTESIAN_POINT('Ctrl Pts',(55.8731107993788,5.70346700526257,330.939996369858));
#72243=CARTESIAN_POINT('Ctrl Pts',(55.5948727651049,-0.327670407549574,
328.006731989914));
#72244=CARTESIAN_POINT('Ctrl Pts',(55.316634730831,-6.05810952376078,331.491086442358));
#72245=CARTESIAN_POINT('Ctrl Pts',(55.0383966965571,-6.2291109475667,338.195519075173));
#72246=CARTESIAN_POINT('Ctrl Pts',(54.760158662283,-0.683749196317659,341.967471018484));
#72247=CARTESIAN_POINT('Ctrl Pts',(54.4819206280093,5.4890791002704,339.345477647838));
#72248=CARTESIAN_POINT('Ctrl Pts',(54.2036825937351,6.62466052521529,332.735703578915));
#72249=CARTESIAN_POINT('Ctrl Pts',(53.9254445594614,1.6808887659992,328.203840914663));
#72250=CARTESIAN_POINT('Ctrl Pts',(53.6472065251873,-4.80540980389684,329.90871313188));
#72251=CARTESIAN_POINT('Ctrl Pts',(53.3689684909135,-6.8818547244892,336.285784160701));
#72252=CARTESIAN_POINT('Ctrl Pts',(53.0907304566394,-2.64292314042703,341.482910043389));
#72253=CARTESIAN_POINT('Ctrl Pts',(52.8124924223656,4.02138000012339,340.730765066856));
#72254=CARTESIAN_POINT('Ctrl Pts',(52.5342543880916,6.99532207003211,334.719581574422));
#72255=CARTESIAN_POINT('Ctrl Pts',(52.2560163538177,3.54976032705684,328.965733932173));
#72256=CARTESIAN_POINT('Ctrl Pts',(51.9777783195437,-3.15336407368193,328.749443194747));
#72257=CARTESIAN_POINT('Ctrl Pts',(51.6995402852698,-6.96269280758023,334.269196179436));
#72258=CARTESIAN_POINT('Ctrl Pts',(51.4213022509958,-4.38246112113954,340.459597043608));
#72259=CARTESIAN_POINT('Ctrl Pts',(51.1430642167219,2.21949045115079,341.639806284384));
#72260=CARTESIAN_POINT('Ctrl Pts',(50.8648261824479,6.78464839604541,336.726763301359));
#72261=CARTESIAN_POINT('Ctrl Pts',(50.5865881481741,5.12363464913532,330.229095123663));
#72262=CARTESIAN_POINT('Ctrl Pts',(50.3083501139,-1.23926299056279,328.109615932539));
#72263=CARTESIAN_POINT('Ctrl Pts',(50.0301120796262,-6.46490727531319,332.313340498224));
#72264=CARTESIAN_POINT('Ctrl Pts',(49.7518740453522,-5.75780157538363,338.982572833658));
#72265=CARTESIAN_POINT('Ctrl Pts',(49.4736360110783,0.233153645263526,341.997056862324));
#72266=CARTESIAN_POINT('Ctrl Pts',(49.1953979768044,6.01014720699452,338.590445084824));
#72267=CARTESIAN_POINT('Ctrl Pts',(48.9171599425304,6.27171738649399,331.888934847865));
#72268=CARTESIAN_POINT('Ctrl Pts',(48.6389219082565,0.777825090804829,328.042403181773));
#72269=CARTESIAN_POINT('Ctrl Pts',(48.3606838739825,-5.42986581003643,330.580755421808));
#72270=CARTESIAN_POINT('Ctrl Pts',(48.0824458397086,-6.65464900169521,337.174583183307));
#72271=CARTESIAN_POINT('Ctrl Pts',(47.8042078054346,-1.7725590269566,341.772828054279));
#72272=CARTESIAN_POINT('Ctrl Pts',(47.5259697711608,4.73618220389178,340.155748586619));
#72273=CARTESIAN_POINT('Ctrl Pts',(47.2477317368866,6.89859893216333,333.807314739742));
#72274=CARTESIAN_POINT('Ctrl Pts',(46.9694937026129,2.73027324354223,328.553390552198));
#72275=CARTESIAN_POINT('Ctrl Pts',(46.6912556683389,-3.94358390191066,329.215424703103));
#72276=CARTESIAN_POINT('Ctrl Pts',(46.413017634065,-6.99847230778318,335.185878223779));
#72277=CARTESIAN_POINT('Ctrl Pts',(46.134779599791,-3.63096597408471,340.98575404205));
#72278=CARTESIAN_POINT('Ctrl Pts',(45.856541565517,3.06862424106128,341.292591725518));
#72279=CARTESIAN_POINT('Ctrl Pts',(45.5783035312431,6.9521832830049,335.824810860979));
#72280=CARTESIAN_POINT('Ctrl Pts',(45.3000654969693,4.45582634019197,329.600113243508));
#72281=CARTESIAN_POINT('Ctrl Pts',(45.0218274626953,-2.12957666712615,328.330812000272));
#72282=CARTESIAN_POINT('Ctrl Pts',(44.7435894284213,-6.76069859952268,333.181726147332));
#72283=CARTESIAN_POINT('Ctrl Pts',(44.4653513941474,-5.187627214885,339.701243371309));
#72284=CARTESIAN_POINT('Ctrl Pts',(44.1871133598734,1.14605309560046,341.906498943672));
#72285=CARTESIAN_POINT('Ctrl Pts',(43.9088753255995,6.42801739596936,337.773762375186));
#72286=CARTESIAN_POINT('Ctrl Pts',(43.6306372913256,5.81108500943841,331.095585015657));
#72287=CARTESIAN_POINT('Ctrl Pts',(43.3523992570517,-0.138594318779784,
328.000431658189));
#72288=CARTESIAN_POINT('Ctrl Pts',(43.0741612227777,-5.9610876863024,331.328678854542));
#72289=CARTESIAN_POINT('Ctrl Pts',(42.7959231885038,-6.3131788696159,338.026043277469));
#72290=CARTESIAN_POINT('Ctrl Pts',(42.5176851542299,-0.87175898665024,341.946452448991));
#72291=CARTESIAN_POINT('Ctrl Pts',(42.2394471199557,5.36966125122276,339.492204737542));
#72292=CARTESIAN_POINT('Ctrl Pts',(41.961209085682,6.68342261491881,332.915527043287));
#72293=CARTESIAN_POINT('Ctrl Pts',(41.6829710514079,1.86390569205994,328.251739414634));
#72294=CARTESIAN_POINT('Ctrl Pts',(41.4047330171342,-4.6660899731994,329.780730921012));
#72295=CARTESIAN_POINT('Ctrl Pts',(41.1264949828601,-6.91408374142877,336.099368624889));
#72296=CARTESIAN_POINT('Ctrl Pts',(40.8482569485863,-2.8171249118577,341.409131968363));
#72297=CARTESIAN_POINT('Ctrl Pts',(40.5700189143122,3.86506786862965,340.8373295031));
#72298=CARTESIAN_POINT('Ctrl Pts',(40.2917808800384,7.00034491438379,334.908695911688));
#72299=CARTESIAN_POINT('Ctrl Pts',(40.0135428457643,3.7115087571295,329.063850734471));
#72300=CARTESIAN_POINT('Ctrl Pts',(39.7353048114905,-2.98332420476309,328.666522120813));
#72301=CARTESIAN_POINT('Ctrl Pts',(39.4570667772165,-6.94040457773766,334.081332674903));
#72302=CARTESIAN_POINT('Ctrl Pts',(39.1788287429426,-4.52837810992604,340.339190673728));
#72303=CARTESIAN_POINT('Ctrl Pts',(38.9005907086686,2.03927411061338,341.697352197598));
#72304=CARTESIAN_POINT('Ctrl Pts',(38.6223526743947,6.73551457947943,336.909452462488));
#72305=CARTESIAN_POINT('Ctrl Pts',(38.3441146401207,5.25067273478944,330.369276386027));
#72306=CARTESIAN_POINT('Ctrl Pts',(38.0658766058468,-1.05263397881429,328.078647020738));
#72307=CARTESIAN_POINT('Ctrl Pts',(37.7876385715729,-6.38995402691219,332.139641125518));
#72308=CARTESIAN_POINT('Ctrl Pts',(37.509400537299,-5.86330758007963,338.825544350581));
#72309=CARTESIAN_POINT('Ctrl Pts',(37.2311625030249,0.0440096907140084,
342.000801990059));
#72310=CARTESIAN_POINT('Ctrl Pts',(36.9529244687511,5.91093991792135,338.751526974927));
#72311=CARTESIAN_POINT('Ctrl Pts',(36.6746864344771,6.35348782778246,332.059531027352));
#72312=CARTESIAN_POINT('Ctrl Pts',(36.3964484002031,0.965533735414213,328.065960054726));
#72313=CARTESIAN_POINT('Ctrl Pts',(36.1182103659293,-5.30847641468909,330.435655193615));
#72314=CARTESIAN_POINT('Ctrl Pts',(35.8399723316553,-6.71097611201565,336.993982191705));
#72315=CARTESIAN_POINT('Ctrl Pts',(35.5617342973813,-1.95491208519051,341.722461163596));
#72316=CARTESIAN_POINT('Ctrl Pts',(35.2834962631074,4.5951459077589,340.281836749019));
#72317=CARTESIAN_POINT('Ctrl Pts',(35.0052582288335,6.92830632540037,333.994148709649));
#72318=CARTESIAN_POINT('Ctrl Pts',(34.7270201945596,2.90346228985566,328.629515553095));
#72319=CARTESIAN_POINT('Ctrl Pts',(34.4487821602856,-3.78584623405643,329.110981945268));
#72320=CARTESIAN_POINT('Ctrl Pts',(34.1705441260117,-7.00093954797376,334.996713284505));
#72321=CARTESIAN_POINT('Ctrl Pts',(33.8923060917377,-3.79137397241392,340.88546079404));
#72322=CARTESIAN_POINT('Ctrl Pts',(33.6140680574638,2.89747953704209,341.373207802144));
#72323=CARTESIAN_POINT('Ctrl Pts',(33.3358300231898,6.92735884208241,336.012356078614));
#72324=CARTESIAN_POINT('Ctrl Pts',(33.057591988916,4.60010318539263,329.72248012409));
#72325=CARTESIAN_POINT('Ctrl Pts',(32.779353954642,-1.94859926712026,328.275706263624));
#72326=CARTESIAN_POINT('Ctrl Pts',(32.5011159203681,-6.70910093347492,332.999717514618));
#72327=CARTESIAN_POINT('Ctrl Pts',(32.2228778860941,-5.31275969934711,339.559358478325));
#72328=CARTESIAN_POINT('Ctrl Pts',(31.9446398518202,0.959022694666936,341.934943462494));
#72329=CARTESIAN_POINT('Ctrl Pts',(31.6664018175462,6.35072411693689,337.946433190731));
#72330=CARTESIAN_POINT('Ctrl Pts',(31.3881637832723,5.91445975362818,331.254024669115));
#72331=CARTESIAN_POINT('Ctrl Pts',(31.1099257489983,0.050582971697756,327.999242418148));
#72332=CARTESIAN_POINT('Ctrl Pts',(30.8316877147243,-5.85971305675627,331.168952069034));
#72333=CARTESIAN_POINT('Ctrl Pts',(30.5534496804505,-6.392636902248,337.854357859992));
#72334=CARTESIAN_POINT('Ctrl Pts',(30.2752116461766,-1.05913221771276,341.920361573089));
#72335=CARTESIAN_POINT('Ctrl Pts',(29.9969736119026,5.24632247025157,339.63565161493));
#72336=CARTESIAN_POINT('Ctrl Pts',(29.7187355776287,6.73730446285876,333.096872591859));
#72337=CARTESIAN_POINT('Ctrl Pts',(29.4404975433547,2.04556159235134,328.30456550112));
#72338=CARTESIAN_POINT('Ctrl Pts',(29.1622595090808,-4.52336295901732,329.656559825556));
#72339=CARTESIAN_POINT('Ctrl Pts',(28.8840214748068,-6.94126408762359,335.912150329029));
#72340=CARTESIAN_POINT('Ctrl Pts',(28.6057834405329,-2.98926961590786,341.330673938871));
#72341=CARTESIAN_POINT('Ctrl Pts',(28.327545406259,3.70593346077893,340.939631515604));
#72342=CARTESIAN_POINT('Ctrl Pts',(28.0493073719851,7.00025609999755,335.097876919286));
#72343=CARTESIAN_POINT('Ctrl Pts',(27.7710693377112,3.8705470398592,329.1663021188));
#72344=CARTESIAN_POINT('Ctrl Pts',(27.4928313034371,-2.81110590957726,328.588225758652));
#72345=CARTESIAN_POINT('Ctrl Pts',(27.2145932691633,-6.9130484576499,333.894139982156));
#72346=CARTESIAN_POINT('Ctrl Pts',(26.9363552348893,-4.67098847256519,340.214885621569));
#72347=CARTESIAN_POINT('Ctrl Pts',(26.6581172006154,1.85756869011575,341.750007697653));
#72348=CARTESIAN_POINT('Ctrl Pts',(26.3798791663414,6.68146248354638,337.090747339552));
#72349=CARTESIAN_POINT('Ctrl Pts',(26.1016411320675,5.37387677405111,330.512839007323));
#72350=CARTESIAN_POINT('Ctrl Pts',(25.8234030977935,-0.865236332699702,
328.052732087688));
#72351=CARTESIAN_POINT('Ctrl Pts',(25.5451650635196,-6.31033482779934,331.968030389673));
#72352=CARTESIAN_POINT('Ctrl Pts',(25.2669270292457,-5.9645321918169,338.665722451259));
#72353=CARTESIAN_POINT('Ctrl Pts',(24.9886889949716,-0.145166399754938,
341.999435125299));
#72354=CARTESIAN_POINT('Ctrl Pts',(24.7104509606978,5.80741645470958,338.909869496345));
#72355=CARTESIAN_POINT('Ctrl Pts',(24.4322129264239,6.43061894601348,332.232274340175));
#72356=CARTESIAN_POINT('Ctrl Pts',(24.1539748921499,1.15253734634087,328.094580170463));
#72357=CARTESIAN_POINT('Ctrl Pts',(23.875736857876,-5.18321076464542,330.293887854488));
#72358=CARTESIAN_POINT('Ctrl Pts',(23.5974988236019,-6.76240286098208,336.811925192347));
#72359=CARTESIAN_POINT('Ctrl Pts',(23.319260789328,-2.1358376646981,341.667185525164));
#72360=CARTESIAN_POINT('Ctrl Pts',(23.0410227550542,4.45075423156706,340.404068109033));
#72361=CARTESIAN_POINT('Ctrl Pts',(22.7627847207802,6.95295466254791,334.18171715316));
#72362=CARTESIAN_POINT('Ctrl Pts',(22.4845466865063,3.07453122515114,328.710292287995));
#72363=CARTESIAN_POINT('Ctrl Pts',(22.2063086522324,-3.62534413756034,329.010839354206));
#72364=CARTESIAN_POINT('Ctrl Pts',(21.9280706179584,-6.99829469522445,334.807550745195));
#72365=CARTESIAN_POINT('Ctrl Pts',(21.6498325836845,-3.94901350574146,340.780869976773));
#72366=CARTESIAN_POINT('Ctrl Pts',(21.3715945494105,2.72421909061666,341.449170156168));
#72367=CARTESIAN_POINT('Ctrl Pts',(21.0933565151366,6.89747603692375,336.199162072843));
#72368=CARTESIAN_POINT('Ctrl Pts',(20.8151184808627,4.74102103072533,329.848700654873));
#72369=CARTESIAN_POINT('Ctrl Pts',(20.5368804465887,-1.76619899801402,328.225510612874));
#72370=CARTESIAN_POINT('Ctrl Pts',(20.2586424123147,-6.65260427533037,332.81916949014));
#72371=CARTESIAN_POINT('Ctrl Pts',(19.9804043780408,-5.4340128014542,339.4141443373));
#72372=CARTESIAN_POINT('Ctrl Pts',(19.7021663437669,0.771292014419021,341.958324078784));
#72373=CARTESIAN_POINT('Ctrl Pts',(19.423928309493,6.26879353291137,338.116952517862));
#72374=CARTESIAN_POINT('Ctrl Pts',(19.145690275219,6.01351575349184,331.415199637444));
#72375=CARTESIAN_POINT('Ctrl Pts',(18.8674522409451,0.239723326439865,328.003165138176));
#72376=CARTESIAN_POINT('Ctrl Pts',(18.5892142066711,-5.75405965897546,331.01202271849));
#72377=CARTESIAN_POINT('Ctrl Pts',(18.3109761723972,-6.46742702513038,337.6805881876));
#72378=CARTESIAN_POINT('Ctrl Pts',(18.0327381381232,-1.24573206938954,341.889217442364));
#72379=CARTESIAN_POINT('Ctrl Pts',(17.7545001038494,5.11915281945485,339.775713534955));
#72380=CARTESIAN_POINT('Ctrl Pts',(17.4762620695754,6.78626672445732,333.279607805933));
#72381=CARTESIAN_POINT('Ctrl Pts',(17.1980240353015,2.2257238215579,328.36228060046));
#72382=CARTESIAN_POINT('Ctrl Pts',(16.9197860010275,-4.37733298075532,329.536290515367));
#72383=CARTESIAN_POINT('Ctrl Pts',(16.6415479667536,-6.96337591595852,335.724265980102));
#72384=CARTESIAN_POINT('Ctrl Pts',(16.3633099324796,-3.15923155234616,341.247593245045));
#72385=CARTESIAN_POINT('Ctrl Pts',(16.0850718982057,3.54409297667212,341.037596403337));
#72386=CARTESIAN_POINT('Ctrl Pts',(15.8068338639318,6.99505569172662,335.286986457062));
#72387=CARTESIAN_POINT('Ctrl Pts',(15.5285958296578,4.02675904533329,329.273013275055));
#72388=CARTESIAN_POINT('Ctrl Pts',(15.2503577953839,-2.63683494209051,328.514611280344));
#72389=CARTESIAN_POINT('Ctrl Pts',(14.9721197611099,-6.88064442278876,333.707754789481));
#72390=CARTESIAN_POINT('Ctrl Pts',(14.693881726836,-4.81018807481828,340.086772654803));
#72391=CARTESIAN_POINT('Ctrl Pts',(14.4156436925621,1.67450687111428,341.797734335452));
#72392=CARTESIAN_POINT('Ctrl Pts',(14.1374056582881,6.62253157717988,337.270515550857));
#72393=CARTESIAN_POINT('Ctrl Pts',(13.8591676240142,5.49315680313418,330.65967815798));
#72394=CARTESIAN_POINT('Ctrl Pts',(13.5809295897403,-0.677206890023213,
328.031890056511));
#72395=CARTESIAN_POINT('Ctrl Pts',(13.3026915554662,-6.22610781625971,331.798633600986));
#72396=CARTESIAN_POINT('Ctrl Pts',(13.0244535211924,-6.06140149577904,338.503223837862));
#72397=CARTESIAN_POINT('Ctrl Pts',(12.7462154869185,-0.334236490530462,
341.992957266009));
#72398=CARTESIAN_POINT('Ctrl Pts',(12.4679774526445,5.69965241209585,339.065357027443));
#72399=CARTESIAN_POINT('Ctrl Pts',(12.1897394183706,6.50305441656604,332.407038648561));
#72400=CARTESIAN_POINT('Ctrl Pts',(11.9115013840966,1.33869937978922,328.128242631365));
#72401=CARTESIAN_POINT('Ctrl Pts',(11.6332633498227,-5.05416034113784,330.155556921528));
#72402=CARTESIAN_POINT('Ctrl Pts',(11.3550253155488,-6.80889167382486,336.628545126353));
#72403=CARTESIAN_POINT('Ctrl Pts',(11.0767872812748,-2.31520369669645,341.607041495793));
#72404=CARTESIAN_POINT('Ctrl Pts',(10.7985492470008,4.30311269193076,340.52235342361));
#72405=CARTESIAN_POINT('Ctrl Pts',(10.5203112127269,6.97252579115532,334.369883087956));
#72406=CARTESIAN_POINT('Ctrl Pts',(10.242073178453,3.2433554259048,328.795661810754));
#72407=CARTESIAN_POINT('Ctrl Pts',(9.96383514417902,-3.46219536102038,328.915069984074));
#72408=CARTESIAN_POINT('Ctrl Pts',(9.6855971099051,-6.99053864265773,334.618528864805));
#72409=CARTESIAN_POINT('Ctrl Pts',(9.40735907563116,-4.10377142576636,340.672057712784));
#72410=CARTESIAN_POINT('Ctrl Pts',(9.12912104135721,2.54897311806734,341.520423791441));
#72411=CARTESIAN_POINT('Ctrl Pts',(8.85088300708329,6.86254969911119,336.385091547203));
#72412=CARTESIAN_POINT('Ctrl Pts',(8.57264497280934,4.87849017425162,329.978684351033));
#72413=CARTESIAN_POINT('Ctrl Pts',(8.29440693853538,-1.58253396617214,328.180258525862));
#72414=CARTESIAN_POINT('Ctrl Pts',(8.01616890426149,-6.59120282966596,332.640219905419));
#72415=CARTESIAN_POINT('Ctrl Pts',(7.7379308699875,-5.55138682090592,339.265695663652));
#72416=CARTESIAN_POINT('Ctrl Pts',(7.45969283571361,0.583165882706493,341.976645094441));
#72417=CARTESIAN_POINT('Ctrl Pts',(7.18145480143964,6.18196872210066,338.285155485332));
#72418=CARTESIAN_POINT('Ctrl Pts',(6.90321676716572,6.10877882471154,331.579068422606));
#72419=CARTESIAN_POINT('Ctrl Pts',(6.62497873289175,0.427558700872944,328.012053184046));
#72420=CARTESIAN_POINT('Ctrl Pts',(6.34674069861787,-5.64206691036484,330.858276072185));
#72421=CARTESIAN_POINT('Ctrl Pts',(6.06850266434387,-6.5415653170953,337.504356491304));
#72422=CARTESIAN_POINT('Ctrl Pts',(5.79026463006997,-1.42345620119259,341.853942631986));
#72423=CARTESIAN_POINT('Ctrl Pts',(5.55839960150834,3.905186457329,340.234875251695));
#72424=CARTESIAN_POINT('Ctrl Pts',(5.37290757865905,5.92636084688762,336.684629902852));
#72425=CARTESIAN_POINT('Ctrl Pts',(5.2801615672344,5.99240691187019,334.662430744869));
#72426=CARTESIAN_POINT('Ctrl Pts',(5.23378856152207,5.77608186237172,333.700728996892));
#72427=CARTESIAN_POINT('Ctrl Pts',(185.616456506696,3.24370764223164,339.546070274699));
#72428=CARTESIAN_POINT('Ctrl Pts',(185.570073697003,4.00077982359114,339.005888754628));
#72429=CARTESIAN_POINT('Ctrl Pts',(185.477317881598,5.22618675040964,337.542420441747));
#72430=CARTESIAN_POINT('Ctrl Pts',(185.291816054769,6.03764046862974,333.775028658698));
#72431=CARTESIAN_POINT('Ctrl Pts',(185.059951026208,3.30915017218641,329.285814453217));
#72432=CARTESIAN_POINT('Ctrl Pts',(184.781712991934,-3.02460665970507,329.125603768544));
#72433=CARTESIAN_POINT('Ctrl Pts',(184.50347495766,-6.57144526074855,334.364156891581));
#72434=CARTESIAN_POINT('Ctrl Pts',(184.225236923386,-4.09364090229947,340.182150482619));
#72435=CARTESIAN_POINT('Ctrl Pts',(183.946998889112,2.14393674640899,341.246697212283));
#72436=CARTESIAN_POINT('Ctrl Pts',(183.668760854838,6.41241529034084,336.577612734481));
#72437=CARTESIAN_POINT('Ctrl Pts',(183.390522820564,4.79718333645851,330.461374221489));
#72438=CARTESIAN_POINT('Ctrl Pts',(183.11228478629,-1.22081282736175,328.509848981737));
#72439=CARTESIAN_POINT('Ctrl Pts',(182.834046752016,-6.11824353328202,332.514407213301));
#72440=CARTESIAN_POINT('Ctrl Pts',(182.555808717742,-5.40118143611244,338.799868456314));
#72441=CARTESIAN_POINT('Ctrl Pts',(182.277570683468,0.272533453155054,341.598293532569));
#72442=CARTESIAN_POINT('Ctrl Pts',(181.999332649194,5.69611223808,338.341537117564));
#72443=CARTESIAN_POINT('Ctrl Pts',(181.72109461492,5.89247205606371,332.018314601662));
#72444=CARTESIAN_POINT('Ctrl Pts',(181.442856580647,0.681387094013621,328.431333780266));
#72445=CARTESIAN_POINT('Ctrl Pts',(181.164618546372,-5.1549913731018,330.872324695149));
#72446=CARTESIAN_POINT('Ctrl Pts',(180.886380512099,-6.26071319068405,337.101220353486));
#72447=CARTESIAN_POINT('Ctrl Pts',(180.608142477824,-1.62106941389026,341.401858145107));
#72448=CARTESIAN_POINT('Ctrl Pts',(180.329904443551,4.50620503883413,339.827604658656));
#72449=CARTESIAN_POINT('Ctrl Pts',(180.051666409277,6.49820206165478,333.823129923343));
#72450=CARTESIAN_POINT('Ctrl Pts',(179.773428375003,2.5268947419063,328.898651332658));
#72451=CARTESIAN_POINT('Ctrl Pts',(179.495190340729,-3.7633064670093,329.573290439871));
#72452=CARTESIAN_POINT('Ctrl Pts',(179.216952306455,-6.59997694026069,335.227940769077));
#72453=CARTESIAN_POINT('Ctrl Pts',(178.938714272181,-3.37994595767685,340.673413241798));
#72454=CARTESIAN_POINT('Ctrl Pts',(178.660476237907,2.94181152473292,340.912478109838));
#72455=CARTESIAN_POINT('Ctrl Pts',(178.382238203633,6.56391200129043,335.725749090934));
#72456=CARTESIAN_POINT('Ctrl Pts',(178.104000169359,4.1624073125058,329.873010839919));
#72457=CARTESIAN_POINT('Ctrl Pts',(177.825762135086,-2.05887712731774,328.725234868675));
#72458=CARTESIAN_POINT('Ctrl Pts',(177.547524100811,-6.39076041776407,333.335718242113));
#72459=CARTESIAN_POINT('Ctrl Pts',(177.269286066538,-4.85793719956362,339.47348842051));
#72460=CARTESIAN_POINT('Ctrl Pts',(176.991048032263,1.13294328325218,341.506004303719));
#72461=CARTESIAN_POINT('Ctrl Pts',(176.71280999799,6.08413843744873,337.568056066012));
#72462=CARTESIAN_POINT('Ctrl Pts',(176.434571963715,5.45200954922573,331.273440680897));
#72463=CARTESIAN_POINT('Ctrl Pts',(176.156333929442,-0.183348030734939,
328.398633779037));
#72464=CARTESIAN_POINT('Ctrl Pts',(175.878095895168,-5.65044982913321,331.581803222127));
#72465=CARTESIAN_POINT('Ctrl Pts',(175.599857860894,-5.93221721982255,337.901801395782));
#72466=CARTESIAN_POINT('Ctrl Pts',(175.32161982662,-0.770076427271954,341.558859259039));
#72467=CARTESIAN_POINT('Ctrl Pts',(175.043381792346,5.0987521362812,339.196948788884));
#72468=CARTESIAN_POINT('Ctrl Pts',(174.765143758072,6.28853112182489,332.983560362031));
#72469=CARTESIAN_POINT('Ctrl Pts',(174.486905723798,1.70741791543838,328.620628828343));
#72470=CARTESIAN_POINT('Ctrl Pts',(174.208667689524,-4.44056751049949,330.111952059519));
#72471=CARTESIAN_POINT('Ctrl Pts',(173.93042965525,-6.51350967472065,336.088964738207));
#72472=CARTESIAN_POINT('Ctrl Pts',(173.652191620976,-2.60910014969608,341.066650549734));
#72473=CARTESIAN_POINT('Ctrl Pts',(173.373953586702,3.68964207244958,340.477060695386));
#72474=CARTESIAN_POINT('Ctrl Pts',(173.095715552428,6.60245422373594,334.861253082165));
#72475=CARTESIAN_POINT('Ctrl Pts',(172.817477518154,3.45629158596449,329.372771467541));
#72476=CARTESIAN_POINT('Ctrl Pts',(172.53923948388,-2.86165882546639,329.048314419396));
#72477=CARTESIAN_POINT('Ctrl Pts',(172.261001449607,-6.5535071707818,334.185631381837));
#72478=CARTESIAN_POINT('Ctrl Pts',(171.982763415333,-4.23129871507806,340.070282405105));
#72479=CARTESIAN_POINT('Ctrl Pts',(171.704525381059,1.97391011758615,341.302010102454));
#72480=CARTESIAN_POINT('Ctrl Pts',(171.426287346785,6.36769077020714,336.750476146298));
#72481=CARTESIAN_POINT('Ctrl Pts',(171.148049312511,4.91793558997074,330.59255606767));
#72482=CARTESIAN_POINT('Ctrl Pts',(170.869811278237,-1.0449364925714,328.479282231975));
#72483=CARTESIAN_POINT('Ctrl Pts',(170.591573243963,-6.04888577911817,332.349974846361));
#72484=CARTESIAN_POINT('Ctrl Pts',(170.313335209689,-5.50186186757595,338.652556429933));
#72485=CARTESIAN_POINT('Ctrl Pts',(170.035097175415,0.0941394724926572,
341.603240889401));
#72486=CARTESIAN_POINT('Ctrl Pts',(169.756859141141,5.60375040815109,338.49422864834));
#72487=CARTESIAN_POINT('Ctrl Pts',(169.478621106867,5.97088230546971,332.178614351428));
#72488=CARTESIAN_POINT('Ctrl Pts',(169.200383072593,0.858623641137144,328.452144020627));
#72489=CARTESIAN_POINT('Ctrl Pts',(168.922145038319,-5.04158126540281,330.7345444759));
#72490=CARTESIAN_POINT('Ctrl Pts',(168.643907004046,-6.31520145830011,336.931290507619));
#72491=CARTESIAN_POINT('Ctrl Pts',(168.365668969771,-1.79345448513614,341.355719746299));
#72492=CARTESIAN_POINT('Ctrl Pts',(168.087430935498,4.37411919769241,339.947598784068));
#72493=CARTESIAN_POINT('Ctrl Pts',(167.809192901223,6.52762825469221,333.999139444138));
#72494=CARTESIAN_POINT('Ctrl Pts',(167.53095486695,2.69082920999616,328.969155063644));
#72495=CARTESIAN_POINT('Ctrl Pts',(167.252716832675,-3.61530408413933,329.473588066119));
#72496=CARTESIAN_POINT('Ctrl Pts',(166.974478798402,-6.60372618206099,335.04952773061));
#72497=CARTESIAN_POINT('Ctrl Pts',(166.696240764128,-3.53200623354396,340.580016527749));
#72498=CARTESIAN_POINT('Ctrl Pts',(166.418002729854,2.78098370316982,340.989806518281));
#72499=CARTESIAN_POINT('Ctrl Pts',(166.13976469558,6.54190594273683,335.902839476387));
#72500=CARTESIAN_POINT('Ctrl Pts',(165.861526661306,4.2994176570277,329.987349972901));
#72501=CARTESIAN_POINT('Ctrl Pts',(165.583288627032,-1.88858275323517,328.671895412691));
#72502=CARTESIAN_POINT('Ctrl Pts',(165.305050592758,-6.34345864628985,333.163649029584));
#72503=CARTESIAN_POINT('Ctrl Pts',(165.026812558484,-4.97703616894048,339.340594827532));
#72504=CARTESIAN_POINT('Ctrl Pts',(164.74857452421,0.956738939712131,341.534240819328));
#72505=CARTESIAN_POINT('Ctrl Pts',(164.470336489937,6.01252884483452,337.731510456463));
#72506=CARTESIAN_POINT('Ctrl Pts',(164.192098455662,5.55070977383256,331.422113264731));
#72507=CARTESIAN_POINT('Ctrl Pts',(163.913860421389,-0.00491372827345363,
328.396089920433));
#72508=CARTESIAN_POINT('Ctrl Pts',(163.635622387114,-5.55602797446947,331.430377382601));
#72509=CARTESIAN_POINT('Ctrl Pts',(163.357384352841,-6.00845735533339,337.740454833212));
#72510=CARTESIAN_POINT('Ctrl Pts',(163.079146318566,-0.947014105893046,
341.535657332433));
#72511=CARTESIAN_POINT('Ctrl Pts',(162.800908284293,4.98349001062004,339.333183563823));
#72512=CARTESIAN_POINT('Ctrl Pts',(162.522670250019,6.34071890057911,333.154211196378));
#72513=CARTESIAN_POINT('Ctrl Pts',(162.244432215745,1.87916364433428,328.669091970219));
#72514=CARTESIAN_POINT('Ctrl Pts',(161.966194181471,-4.30687235190619,329.99375359894));
#72515=CARTESIAN_POINT('Ctrl Pts',(161.687956147197,-6.54055516013407,335.912573657838));
#72516=CARTESIAN_POINT('Ctrl Pts',(161.409718112923,-2.77206703634281,340.993938340504));
#72517=CARTESIAN_POINT('Ctrl Pts',(161.131480078649,3.54030609105783,340.574754278473));
#72518=CARTESIAN_POINT('Ctrl Pts',(160.853242044375,6.60379257352697,335.039700498327));
#72519=CARTESIAN_POINT('Ctrl Pts',(160.575004010101,3.60707608308904,329.468214156844));
#72520=CARTESIAN_POINT('Ctrl Pts',(160.296765975827,-2.69980088844387,328.9731660346));
#72521=CARTESIAN_POINT('Ctrl Pts',(160.018527941553,-6.52911043364773,334.008854486481));
#72522=CARTESIAN_POINT('Ctrl Pts',(159.740289907279,-4.36675170340512,339.954102546833));
#72523=CARTESIAN_POINT('Ctrl Pts',(159.462051873005,1.80291061190286,341.353043822392));
#72524=CARTESIAN_POINT('Ctrl Pts',(159.183813838731,6.31806846958463,336.921890552913));
#72525=CARTESIAN_POINT('Ctrl Pts',(158.905575804457,5.0352281472663,330.727046690085));
#72526=CARTESIAN_POINT('Ctrl Pts',(158.627337770184,-0.868366725952659,
328.453429011078));
#72527=CARTESIAN_POINT('Ctrl Pts',(158.34909973591,-5.97507427183675,332.187502901376));
#72528=CARTESIAN_POINT('Ctrl Pts',(158.070861701636,-5.59854435040793,338.502563866691));
#72529=CARTESIAN_POINT('Ctrl Pts',(157.792623667362,-0.0843129129889187,
341.603373669303));
#72530=CARTESIAN_POINT('Ctrl Pts',(157.514385633088,5.50729124022346,338.64436492123));
#72531=CARTESIAN_POINT('Ctrl Pts',(157.236147598814,6.04493550976823,332.340976275684));
#72532=CARTESIAN_POINT('Ctrl Pts',(156.95790956454,1.03523168510056,328.477734454815));
#72533=CARTESIAN_POINT('Ctrl Pts',(156.679671530266,-4.92448897698921,330.599879456282));
#72534=CARTESIAN_POINT('Ctrl Pts',(156.401433495992,-6.36507879023421,336.759950135045));
#72535=CARTESIAN_POINT('Ctrl Pts',(156.123195461718,-1.96452974609034,341.3049405517));
#72536=CARTESIAN_POINT('Ctrl Pts',(155.844957427444,4.23883924962917,340.063980084828));
#72537=CARTESIAN_POINT('Ctrl Pts',(155.56671939317,6.55228803112875,334.175879838335));
#72538=CARTESIAN_POINT('Ctrl Pts',(155.288481358896,2.85279879807429,329.044062500207));
#72539=CARTESIAN_POINT('Ctrl Pts',(155.010243324622,-3.46466178473171,329.377921096147));
#72540=CARTESIAN_POINT('Ctrl Pts',(154.732005290348,-6.60265338601353,334.871078520404));
#72541=CARTESIAN_POINT('Ctrl Pts',(154.453767256075,-3.68148742995497,340.482545283609));
#72542=CARTESIAN_POINT('Ctrl Pts',(154.1755292218,2.61812520190787,341.062761162283));
#72543=CARTESIAN_POINT('Ctrl Pts',(153.897291187527,6.5151229794445,336.079270608537));
#72544=CARTESIAN_POINT('Ctrl Pts',(153.619053153253,4.43328856180245,330.105349347346));
#72545=CARTESIAN_POINT('Ctrl Pts',(153.340815118979,-1.7169093337738,328.62317674517));
#72546=CARTESIAN_POINT('Ctrl Pts',(153.062577084705,-6.29152487528601,332.992920722196));
#72547=CARTESIAN_POINT('Ctrl Pts',(152.784339050431,-5.0925009015033,339.204531728019));
#72548=CARTESIAN_POINT('Ctrl Pts',(152.506101016157,0.779835984398815,341.557706025828));
#72549=CARTESIAN_POINT('Ctrl Pts',(152.227862981883,5.93652889777846,337.892970295316));
#72550=CARTESIAN_POINT('Ctrl Pts',(151.949624947609,5.64535686468971,331.573398424964));
#72551=CARTESIAN_POINT('Ctrl Pts',(151.671386913335,0.173524162205951,328.398368243467));
#72552=CARTESIAN_POINT('Ctrl Pts',(151.393148879061,-5.45754910272178,331.281558085015));
#72553=CARTESIAN_POINT('Ctrl Pts',(151.114910844787,-6.08031010937444,337.577107187832));
#72554=CARTESIAN_POINT('Ctrl Pts',(150.836672810513,-1.12326027388429,341.507683062416));
#72555=CARTESIAN_POINT('Ctrl Pts',(150.558434776239,4.86458893565501,339.466254243865));
#72556=CARTESIAN_POINT('Ctrl Pts',(150.280196741966,6.38827668015871,333.326209827524));
#72557=CARTESIAN_POINT('Ctrl Pts',(150.001958707691,2.04953720609002,328.722177947362));
#72558=CARTESIAN_POINT('Ctrl Pts',(149.723720673418,-4.17003231088781,329.879210704404));
#72559=CARTESIAN_POINT('Ctrl Pts',(149.445482639144,-6.56282472574003,335.735516215289));
#72560=CARTESIAN_POINT('Ctrl Pts',(149.16724460487,-2.93300975691482,340.916849351605));
#72561=CARTESIAN_POINT('Ctrl Pts',(148.889006570596,3.38838497467808,340.668377170506));
#72562=CARTESIAN_POINT('Ctrl Pts',(148.610768536322,6.60030882748914,335.218118925144));
#72563=CARTESIAN_POINT('Ctrl Pts',(148.332530502048,3.75522668971203,329.567696161608));
#72564=CARTESIAN_POINT('Ctrl Pts',(148.054292467774,-2.53597155415873,328.90241844989));
#72565=CARTESIAN_POINT('Ctrl Pts',(147.7760544335,-6.49994613365681,333.832801326553));
#72566=CARTESIAN_POINT('Ctrl Pts',(147.497816399226,-4.4990160853457,339.834305198013));
#72567=CARTESIAN_POINT('Ctrl Pts',(147.219578364952,1.63059461911859,341.399438543485));
#72568=CARTESIAN_POINT('Ctrl Pts',(146.941340330678,6.26383270915488,337.091901593159));
#72569=CARTESIAN_POINT('Ctrl Pts',(146.663102296404,5.14884397601897,330.864657427207));
#72570=CARTESIAN_POINT('Ctrl Pts',(146.38486426213,-0.691162877096977,328.432356102752));
#72571=CARTESIAN_POINT('Ctrl Pts',(146.106626227856,-5.89689975944835,332.027084644536));
#72572=CARTESIAN_POINT('Ctrl Pts',(145.828388193583,-5.69113877065188,338.350013727871));
#72573=CARTESIAN_POINT('Ctrl Pts',(145.550150159308,-0.26270373309874,341.59868465926));
#72574=CARTESIAN_POINT('Ctrl Pts',(145.271912125034,5.40681064281838,338.791840075272));
#72575=CARTESIAN_POINT('Ctrl Pts',(144.993674090761,6.11457469621534,332.505279821676));
#72576=CARTESIAN_POINT('Ctrl Pts',(144.715436056487,1.21108380187007,328.508087453717));
#72577=CARTESIAN_POINT('Ctrl Pts',(144.437198022213,-4.80380082188375,330.468427409011));
#72578=CARTESIAN_POINT('Ctrl Pts',(144.158959987939,-6.41030833537875,336.587324645153));
#72579=CARTESIAN_POINT('Ctrl Pts',(143.880721953665,-2.13417050549261,341.249557483312));
#72580=CARTESIAN_POINT('Ctrl Pts',(143.602483919391,4.10046409697908,340.176663662353));
#72581=CARTESIAN_POINT('Ctrl Pts',(143.324245885117,6.57216332040393,334.353222005882));
#72582=CARTESIAN_POINT('Ctrl Pts',(143.046007850843,3.01268526966569,329.123318968187));
#72583=CARTESIAN_POINT('Ctrl Pts',(142.767769816569,-3.31148958588299,329.286359373715));
#72584=CARTESIAN_POINT('Ctrl Pts',(142.489531782295,-6.59675932597306,334.692723448789));
#72585=CARTESIAN_POINT('Ctrl Pts',(142.211293748021,-3.82828040062582,340.381070679513));
#72586=CARTESIAN_POINT('Ctrl Pts',(141.933055713747,2.45335494304968,341.131288772122));
#72587=CARTESIAN_POINT('Ctrl Pts',(141.654817679474,6.48358266694808,336.254913656228));
#72588=CARTESIAN_POINT('Ctrl Pts',(141.376579645199,4.56392227491153,330.226922800509));
#72589=CARTESIAN_POINT('Ctrl Pts',(141.098341610926,-1.54398222542898,328.579114440258));
#72590=CARTESIAN_POINT('Ctrl Pts',(140.820103576652,-6.2349970266336,332.823657986068));
#72591=CARTESIAN_POINT('Ctrl Pts',(140.541865542377,-5.20424708490183,339.065398475307));
#72592=CARTESIAN_POINT('Ctrl Pts',(140.263627508104,0.602363592083287,341.57638278894));
#72593=CARTESIAN_POINT('Ctrl Pts',(139.98538947383,5.85619409148563,338.052317684414));
#72594=CARTESIAN_POINT('Ctrl Pts',(139.707151439556,5.7358817104147,331.727185693036));
#72595=CARTESIAN_POINT('Ctrl Pts',(139.428913405282,0.351835345171481,328.405467084499));
#72596=CARTESIAN_POINT('Ctrl Pts',(139.150675371008,-5.35508512325443,331.135453997371));
#72597=CARTESIAN_POINT('Ctrl Pts',(138.872437336734,-6.14772301499658,337.41187773625));
#72598=CARTESIAN_POINT('Ctrl Pts',(138.59419930246,-1.29868623611949,341.47495687583));
#72599=CARTESIAN_POINT('Ctrl Pts',(138.315961268186,4.74213573306708,339.596063660667));
#72600=CARTESIAN_POINT('Ctrl Pts',(138.037723233912,6.43116973382671,333.499430661899));
#72601=CARTESIAN_POINT('Ctrl Pts',(137.759485199638,2.21841419376326,328.779847996339));
#72602=CARTESIAN_POINT('Ctrl Pts',(137.481247165364,-4.03014730817692,329.768407015246));
#72603=CARTESIAN_POINT('Ctrl Pts',(137.203009131091,-6.58030211027989,335.557921698075));
#72604=CARTESIAN_POINT('Ctrl Pts',(136.924771096816,-3.09181079087896,340.835439873493));
#72605=CARTESIAN_POINT('Ctrl Pts',(136.646533062543,3.23398965625914,340.757861007957));
#72606=CARTESIAN_POINT('Ctrl Pts',(136.368295028268,6.59200552945729,335.396378081309));
#72607=CARTESIAN_POINT('Ctrl Pts',(136.090056993995,3.90063522611462,329.671144839975));
#72608=CARTESIAN_POINT('Ctrl Pts',(135.811818959721,-2.37029045095188,328.836123325223));
#72609=CARTESIAN_POINT('Ctrl Pts',(135.533580925447,-6.46603556660954,333.657600456243));
#72610=CARTESIAN_POINT('Ctrl Pts',(135.255342891173,-4.62799528131817,339.710977834784));
#72611=CARTESIAN_POINT('Ctrl Pts',(134.977104856899,1.45708796454039,341.441160388263));
#72612=CARTESIAN_POINT('Ctrl Pts',(134.698866822625,6.20502309192341,337.260385124804));
#72613=CARTESIAN_POINT('Ctrl Pts',(134.420628788351,5.25870011383906,331.005287795542));
#72614=CARTESIAN_POINT('Ctrl Pts',(134.142390754077,-0.513454340428938,
328.416078894456));
#72615=CARTESIAN_POINT('Ctrl Pts',(133.864152719803,-5.81441932505895,331.868837213412));
#72616=CARTESIAN_POINT('Ctrl Pts',(133.585914685529,-5.77957751577092,338.195017405732));
#72617=CARTESIAN_POINT('Ctrl Pts',(133.307676651255,-0.440902726684218,
341.589177283193));
#72618=CARTESIAN_POINT('Ctrl Pts',(133.029438616981,5.30238198696701,338.936546423964));
#72619=CARTESIAN_POINT('Ctrl Pts',(132.751200582707,6.17974901420846,332.671405014795));
#72620=CARTESIAN_POINT('Ctrl Pts',(132.472962548433,1.38605158405674,328.543180853541));
#72621=CARTESIAN_POINT('Ctrl Pts',(132.194724514159,-4.67960492669601,330.3402843205));
#72622=CARTESIAN_POINT('Ctrl Pts',(131.916486479886,-6.45085706707532,336.413540089245));
#72623=CARTESIAN_POINT('Ctrl Pts',(131.638248445611,-2.30225289149384,341.189610981908));
#72624=CARTESIAN_POINT('Ctrl Pts',(131.360010411338,3.9590947814145,340.285567234982));
#72625=CARTESIAN_POINT('Ctrl Pts',(131.081772377064,6.58723960956198,334.531036451358));
#72626=CARTESIAN_POINT('Ctrl Pts',(130.80353434279,3.17037187551183,329.206866594432));
#72627=CARTESIAN_POINT('Ctrl Pts',(130.525296308516,-3.1558993340834,329.198969757288));
#72628=CARTESIAN_POINT('Ctrl Pts',(130.247058274242,-6.58604830578809,334.514592750813));
#72629=CARTESIAN_POINT('Ctrl Pts',(129.968820239968,-3.97227795718472,340.275666812319));
#72630=CARTESIAN_POINT('Ctrl Pts',(129.690582205694,2.28679324200054,341.195339308874));
#72631=CARTESIAN_POINT('Ctrl Pts',(129.41234417142,6.44730803601481,336.429640364734));
#72632=CARTESIAN_POINT('Ctrl Pts',(129.134106137146,4.69122340748892,330.351981559335));
#72633=CARTESIAN_POINT('Ctrl Pts',(128.855868102872,-1.36992769974558,328.539740672295));
#72634=CARTESIAN_POINT('Ctrl Pts',(128.577630068598,-6.17391637702325,332.655984417018));
#72635=CARTESIAN_POINT('Ctrl Pts',(128.299392034324,-5.31219312196306,338.923296664632));
#72636=CARTESIAN_POINT('Ctrl Pts',(128.021154000051,0.424451353280695,341.590257470875));
#72637=CARTESIAN_POINT('Ctrl Pts',(127.742915965776,5.77158308651039,338.209436268139));
#72638=CARTESIAN_POINT('Ctrl Pts',(127.464677931503,5.82221820967631,331.883362773332));
#72639=CARTESIAN_POINT('Ctrl Pts',(127.186439897228,0.529889617622296,328.417381259949));
#72640=CARTESIAN_POINT('Ctrl Pts',(126.908201862955,-5.24871085536584,330.992171805017));
#72641=CARTESIAN_POINT('Ctrl Pts',(126.629963828681,-6.21064684722995,337.244887129174));
#72642=CARTESIAN_POINT('Ctrl Pts',(126.351725794407,-1.47316389638836,341.437502669367));
#72643=CARTESIAN_POINT('Ctrl Pts',(126.073487760133,4.61621981830537,339.722517027267));
#72644=CARTESIAN_POINT('Ctrl Pts',(125.795249725859,6.46936674103309,333.67374721348));
#72645=CARTESIAN_POINT('Ctrl Pts',(125.517011691585,2.38567129321132,328.842060006424));
#72646=CARTESIAN_POINT('Ctrl Pts',(125.238773657311,-3.88731948793991,329.661423440427));
#72647=CARTESIAN_POINT('Ctrl Pts',(124.960535623037,-6.59297455175028,335.37991978589));
#72648=CARTESIAN_POINT('Ctrl Pts',(124.682297588763,-3.24835418156428,340.749769351449));
#72649=CARTESIAN_POINT('Ctrl Pts',(124.404059554489,3.07723287541413,340.843140449638));
#72650=CARTESIAN_POINT('Ctrl Pts',(124.125821520215,6.57888874250778,335.574347801809));
#72651=CARTESIAN_POINT('Ctrl Pts',(123.847583485941,4.04319551484074,329.778484653617));
#72652=CARTESIAN_POINT('Ctrl Pts',(123.569345451667,-2.20287855932757,328.774329069363));
#72653=CARTESIAN_POINT('Ctrl Pts',(123.291107417393,-6.42740349403529,333.4833798074));
#72654=CARTESIAN_POINT('Ctrl Pts',(123.012869383119,-4.75359511058692,339.584210510911));
#72655=CARTESIAN_POINT('Ctrl Pts',(122.734631348846,1.28251734289823,341.478178891393));
#72656=CARTESIAN_POINT('Ctrl Pts',(122.456393314572,6.14168256073063,337.427218121009));
#72657=CARTESIAN_POINT('Ctrl Pts',(122.178155280298,5.36471634366653,331.148835106654));
#72658=CARTESIAN_POINT('Ctrl Pts',(121.899917246024,-0.335370878896913,
328.404609271823));
#72659=CARTESIAN_POINT('Ctrl Pts',(121.62167921175,-5.72769319596271,331.712876160432));
#72660=CARTESIAN_POINT('Ctrl Pts',(121.343441177476,-5.86379600770653,338.037688078744));
#72661=CARTESIAN_POINT('Ctrl Pts',(121.065203143202,-0.61877977266526,341.574858483396));
#72662=CARTESIAN_POINT('Ctrl Pts',(120.786965108928,5.19408152657644,339.078378302588));
#72663=CARTESIAN_POINT('Ctrl Pts',(120.508727074654,6.24041087339662,332.83923055026));
#72664=CARTESIAN_POINT('Ctrl Pts',(120.23048904038,1.56000727001425,328.582989029054));
#72665=CARTESIAN_POINT('Ctrl Pts',(119.952251006106,-4.55199197939054,330.215543760959));
#72666=CARTESIAN_POINT('Ctrl Pts',(119.674012971832,-6.48669537660025,336.238723364973));
#72667=CARTESIAN_POINT('Ctrl Pts',(119.395774937558,-2.46865417017073,341.125144820479));
#72668=CARTESIAN_POINT('Ctrl Pts',(119.117536903284,3.81483453094864,340.39061128122));
#72669=CARTESIAN_POINT('Ctrl Pts',(118.83929886901,6.59750588988183,334.709193334478));
#72670=CARTESIAN_POINT('Ctrl Pts',(118.561060834736,3.32574347269777,329.294644372386));
#72671=CARTESIAN_POINT('Ctrl Pts',(118.282822800463,-2.99800464148784,329.115816058845));
#72672=CARTESIAN_POINT('Ctrl Pts',(118.004584766188,-6.57052814665602,334.336816497688));
#72673=CARTESIAN_POINT('Ctrl Pts',(117.726346731915,-4.11337495247446,340.166410648031));
#72674=CARTESIAN_POINT('Ctrl Pts',(117.448108697641,2.11856172227814,341.254866002772));
#72675=CARTESIAN_POINT('Ctrl Pts',(117.169870663367,6.40632557441585,336.603323148441));
#72676=CARTESIAN_POINT('Ctrl Pts',(116.891632629093,4.81509900412262,330.480434305795));
#72677=CARTESIAN_POINT('Ctrl Pts',(116.613394594819,-1.19487285150915,328.505084192042));
#72678=CARTESIAN_POINT('Ctrl Pts',(116.335156560545,-6.10832752760533,332.490022450452));
#72679=CARTESIAN_POINT('Ctrl Pts',(116.056918526271,-5.41626019038464,338.778330058875));
#72680=CARTESIAN_POINT('Ctrl Pts',(115.778680491997,0.246229179682688,341.599319940328));
#72681=CARTESIAN_POINT('Ctrl Pts',(115.500442457723,5.68275766589193,338.364211318346));
#72682=CARTESIAN_POINT('Ctrl Pts',(115.222204423449,5.90430331947782,332.041815625194));
#72683=CARTESIAN_POINT('Ctrl Pts',(114.943966389175,0.707556964153051,328.434102070073));
#72684=CARTESIAN_POINT('Ctrl Pts',(114.665728354901,-5.13850397365131,330.851816132751));
#72685=CARTESIAN_POINT('Ctrl Pts',(114.387490320627,-6.26903565903015,337.076257303309));
#72686=CARTESIAN_POINT('Ctrl Pts',(114.109252286354,-1.64656585093195,341.395347792128));
#72687=CARTESIAN_POINT('Ctrl Pts',(113.831014252079,4.48693313529438,339.84552200729));
#72688=CARTESIAN_POINT('Ctrl Pts',(113.552776217806,6.50283981028572,333.849032196149));
#72689=CARTESIAN_POINT('Ctrl Pts',(113.274538183532,2.55118637313611,328.908768550345));
#72690=CARTESIAN_POINT('Ctrl Pts',(112.996300149258,-3.74165314319136,329.558338099461));
#72691=CARTESIAN_POINT('Ctrl Pts',(112.718062114984,-6.60083279672198,335.201640455903));
#72692=CARTESIAN_POINT('Ctrl Pts',(112.43982408071,-3.40252562083322,340.659900342171));
#72693=CARTESIAN_POINT('Ctrl Pts',(112.161586046436,2.91822909609835,340.924153224421));
#72694=CARTESIAN_POINT('Ctrl Pts',(111.883348012162,6.56096804453132,335.751898132978));
#72695=CARTESIAN_POINT('Ctrl Pts',(111.605109977888,4.18280345822748,329.8896372229));
#72696=CARTESIAN_POINT('Ctrl Pts',(111.326871943614,-2.03385812361386,328.717080804535));
#72697=CARTESIAN_POINT('Ctrl Pts',(111.04863390934,-6.38407812511147,333.310266596113));
#72698=CARTESIAN_POINT('Ctrl Pts',(110.770395875066,-4.87572386003294,339.454095792015));
#72699=CARTESIAN_POINT('Ctrl Pts',(110.492157840792,1.10701022583161,341.51046702193));
#72700=CARTESIAN_POINT('Ctrl Pts',(110.213919806518,6.07385736689464,337.592278760157));
#72701=CARTESIAN_POINT('Ctrl Pts',(109.935681772244,5.46681525234625,331.295194542159));
#72702=CARTESIAN_POINT('Ctrl Pts',(109.657443737971,-0.157042529219445,
328.397955609983));
#72703=CARTESIAN_POINT('Ctrl Pts',(109.379205703697,-5.63678469966438,331.559315368511));
#72704=CARTESIAN_POINT('Ctrl Pts',(109.100967669423,-5.94373275003311,337.878140628934));
#72705=CARTESIAN_POINT('Ctrl Pts',(108.822729635149,-0.796204985048034,
341.555738715471));
#72706=CARTESIAN_POINT('Ctrl Pts',(108.544491600875,5.08198834274931,339.217232145364));
#72707=CARTESIAN_POINT('Ctrl Pts',(108.266253566601,6.29651597843058,333.008633881702));
#72708=CARTESIAN_POINT('Ctrl Pts',(107.988015532327,1.73282383712962,328.627482912285));
#72709=CARTESIAN_POINT('Ctrl Pts',(107.709777498053,-4.42105516306729,330.094296816067));
#72710=CARTESIAN_POINT('Ctrl Pts',(107.431539463779,-6.51779709478459,336.063002123683));
#72711=CARTESIAN_POINT('Ctrl Pts',(107.153301429505,-2.63325283514557,341.056206072282));
#72712=CARTESIAN_POINT('Ctrl Pts',(106.875063395231,3.66778868455823,340.491719097801));
#72713=CARTESIAN_POINT('Ctrl Pts',(106.596825360957,6.60295466491539,334.887562564912));
#72714=CARTESIAN_POINT('Ctrl Pts',(106.318587326683,3.47868660873086,329.386588206628));
#72715=CARTESIAN_POINT('Ctrl Pts',(106.040349292409,-2.8379208029558,329.036958997299));
#72716=CARTESIAN_POINT('Ctrl Pts',(105.762111258135,-6.55021018141231,334.159524501809));
#72717=CARTESIAN_POINT('Ctrl Pts',(105.483873223861,-4.25146835733054,340.05338196561));
#72718=CARTESIAN_POINT('Ctrl Pts',(105.205635189587,1.94878322670338,341.309825387367));
#72719=CARTESIAN_POINT('Ctrl Pts',(104.927397155314,6.36066520758488,336.775835184007));
#72720=CARTESIAN_POINT('Ctrl Pts',(104.649159121039,4.93545861073031,330.612187243568));
#72721=CARTESIAN_POINT('Ctrl Pts',(104.370921086766,-1.01894550594178,328.475170305697));
#72722=CARTESIAN_POINT('Ctrl Pts',(104.092683052492,-6.03827837142212,332.325893271959));
#72723=CARTESIAN_POINT('Ctrl Pts',(103.814445018218,-5.51637230029104,338.630604512794));
#72724=CARTESIAN_POINT('Ctrl Pts',(103.536206983944,0.0678272092954339,
341.603563579873));
#72725=CARTESIAN_POINT('Ctrl Pts',(103.25796894967,5.58978269003947,338.51652981814));
#72726=CARTESIAN_POINT('Ctrl Pts',(102.979730915396,5.98207710119154,332.202428546197));
#72727=CARTESIAN_POINT('Ctrl Pts',(102.701492881122,0.884707651893417,328.45561730532));
#72728=CARTESIAN_POINT('Ctrl Pts',(102.423254846848,-5.02454495128375,330.714489468422));
#72729=CARTESIAN_POINT('Ctrl Pts',(102.145016812574,-6.32284681482974,336.906111392321));
#72730=CARTESIAN_POINT('Ctrl Pts',(101.8667787783,-1.81876548147248,341.348523025644));
#72731=CARTESIAN_POINT('Ctrl Pts',(101.588540744026,4.35437008929757,339.964988782382));
#72732=CARTESIAN_POINT('Ctrl Pts',(101.310302709752,6.5315644995164,334.02515761664));
#72733=CARTESIAN_POINT('Ctrl Pts',(101.032064675478,2.71483857426302,328.979924917459));
#72734=CARTESIAN_POINT('Ctrl Pts',(100.753826641205,-3.59325463963987,329.459226265363));
#72735=CARTESIAN_POINT('Ctrl Pts',(100.47558860693,-6.60387110709679,335.023213887857));
#72736=CARTESIAN_POINT('Ctrl Pts',(100.197350572657,-3.55421253254876,340.565898468101));
#72737=CARTESIAN_POINT('Ctrl Pts',(99.9191125383824,2.7570944230283,341.000840176695));
#72738=CARTESIAN_POINT('Ctrl Pts',(99.640874504109,6.53825652123917,335.928899427393));
#72739=CARTESIAN_POINT('Ctrl Pts',(99.3626364698346,4.31935711441718,330.004521384104));
#72740=CARTESIAN_POINT('Ctrl Pts',(99.0843984355609,-1.86335256269885,328.664420333481));
#72741=CARTESIAN_POINT('Ctrl Pts',(98.8061604012869,-6.336091096065,333.138387229819));
#72742=CARTESIAN_POINT('Ctrl Pts',(98.527922367013,-4.99429235112359,339.320728687994));
#72743=CARTESIAN_POINT('Ctrl Pts',(98.2496843327389,0.930694768809688,341.538001203048));
#72744=CARTESIAN_POINT('Ctrl Pts',(97.9714462984651,6.00159703643856,337.755446514805));
#72745=CARTESIAN_POINT('Ctrl Pts',(97.6932082641911,5.56492228715485,331.44425923025));
#72746=CARTESIAN_POINT('Ctrl Pts',(97.4149702299172,0.0214004930674214,
328.396122767447));
#72747=CARTESIAN_POINT('Ctrl Pts',(97.1367321956432,-5.5417602176372,331.40826696789));
#72748=CARTESIAN_POINT('Ctrl Pts',(96.8584941613693,-6.01932937286292,337.716491558008));
#72749=CARTESIAN_POINT('Ctrl Pts',(96.5802561270954,-0.973048807768221,
341.531831940691));
#72750=CARTESIAN_POINT('Ctrl Pts',(96.3020180928214,4.96618428603849,339.353006561085));
#72751=CARTESIAN_POINT('Ctrl Pts',(96.0237800585475,6.34802336130759,333.179491310641));
#72752=CARTESIAN_POINT('Ctrl Pts',(95.7455420242736,1.90437509457594,328.676630013759));
#72753=CARTESIAN_POINT('Ctrl Pts',(95.4673039899995,-4.28689008791774,329.976632020462));
#72754=CARTESIAN_POINT('Ctrl Pts',(95.1890659557258,-6.54413951112327,335.886504677198));
#72755=CARTESIAN_POINT('Ctrl Pts',(94.9108279214516,-2.79592869631185,340.982845076456));
#72756=CARTESIAN_POINT('Ctrl Pts',(94.6325898871779,3.51806461526506,340.588816855701));
#72757=CARTESIAN_POINT('Ctrl Pts',(94.3543518529038,6.60358195596182,335.066013897269));
#72758=CARTESIAN_POINT('Ctrl Pts',(94.0761138186299,3.62908960438232,329.482630959679));
#72759=CARTESIAN_POINT('Ctrl Pts',(93.797875784356,-2.67576471186408,328.962456154156));
#72760=CARTESIAN_POINT('Ctrl Pts',(93.519637750082,-6.52510924625522,333.982846221964));
#72761=CARTESIAN_POINT('Ctrl Pts',(93.2413997158082,-4.38645733581255,339.93666329871));
#72762=CARTESIAN_POINT('Ctrl Pts',(92.9631616815341,1.77758172770115,341.360177331261));
#72763=CARTESIAN_POINT('Ctrl Pts',(92.6849236472602,6.3103602767668,336.947050502976));
#72764=CARTESIAN_POINT('Ctrl Pts',(92.4066856129864,5.05221434060857,330.747144166529));
#72765=CARTESIAN_POINT('Ctrl Pts',(92.1284475787124,-0.842274125364607,
328.450020856409));
#72766=CARTESIAN_POINT('Ctrl Pts',(91.8502095444384,-5.96382005843634,332.163716728827));
#72767=CARTESIAN_POINT('Ctrl Pts',(91.5719715101645,-5.61245634972109,338.48022789573));
#72768=CARTESIAN_POINT('Ctrl Pts',(91.2937334758905,-0.110624288586713,
341.602985290799));
#72769=CARTESIAN_POINT('Ctrl Pts',(91.0154954416166,5.49272604937187,338.666280544406));
#72770=CARTESIAN_POINT('Ctrl Pts',(90.7372574073426,6.05548276432548,332.365084256623));
#72771=CARTESIAN_POINT('Ctrl Pts',(90.4590193730688,1.0612123252367,328.481911255245));
#72772=CARTESIAN_POINT('Ctrl Pts',(90.1807813387946,-4.90691700125357,330.580292088096));
#72773=CARTESIAN_POINT('Ctrl Pts',(89.902543304521,-6.37204102166964,336.734573636919));
#72774=CARTESIAN_POINT('Ctrl Pts',(89.6243052702468,-1.9896370476708,341.297062561407));
#72775=CARTESIAN_POINT('Ctrl Pts',(89.346067235973,4.21862747798084,340.080830117783));
#72776=CARTESIAN_POINT('Ctrl Pts',(89.067829201699,6.55551983392898,334.201994867998));
#72777=CARTESIAN_POINT('Ctrl Pts',(88.7895911674251,2.87650839759463,329.055477149316));
#72778=CARTESIAN_POINT('Ctrl Pts',(88.5113531331511,-3.44223233801797,329.364160309692));
#72779=CARTESIAN_POINT('Ctrl Pts',(88.2331150988773,-6.60208726429748,334.844770369007));
#72780=CARTESIAN_POINT('Ctrl Pts',(87.9548770646033,-3.7033041547795,340.467832369498));
#72781=CARTESIAN_POINT('Ctrl Pts',(87.6766390303294,2.59394651689991,341.073145309574));
#72782=CARTESIAN_POINT('Ctrl Pts',(87.3984009960554,6.5107707566081,336.105222438532));
#72783=CARTESIAN_POINT('Ctrl Pts',(87.1201629617815,4.45275677179588,330.123053248705));
#72784=CARTESIAN_POINT('Ctrl Pts',(86.8419249275075,-1.6914863799112,328.616386108926));
#72785=CARTESIAN_POINT('Ctrl Pts',(86.5636868932336,-6.28347744707182,332.967867214998));
#72786=CARTESIAN_POINT('Ctrl Pts',(86.2854488589596,-5.10921400502972,339.184206583637));
#72787=CARTESIAN_POINT('Ctrl Pts',(86.0072108246857,0.753699717553054,341.560761329258));
#72788=CARTESIAN_POINT('Ctrl Pts',(85.7289727904118,5.92495433392699,337.916602239699));
#72789=CARTESIAN_POINT('Ctrl Pts',(85.4507347561379,5.65896581023874,331.595920323747));
#72790=CARTESIAN_POINT('Ctrl Pts',(85.1724967218639,0.199827888692849,328.399112082556));
#72791=CARTESIAN_POINT('Ctrl Pts',(84.89425868759,-5.44268913685168,331.25984125426));
#72792=CARTESIAN_POINT('Ctrl Pts',(84.616020653316,-6.09053067546736,337.552858902275));
#72793=CARTESIAN_POINT('Ctrl Pts',(84.3377826190421,-1.14918210929235,341.503155615808));
#72794=CARTESIAN_POINT('Ctrl Pts',(84.0595445847682,4.84675391668017,339.485602407134));
#72795=CARTESIAN_POINT('Ctrl Pts',(83.7813065504942,6.39489541128596,333.351678076816));
#72796=CARTESIAN_POINT('Ctrl Pts',(83.5030685162203,2.07453577545617,328.730394446212));
#72797=CARTESIAN_POINT('Ctrl Pts',(83.2248304819463,-4.14959472141189,329.862635293094));
#72798=CARTESIAN_POINT('Ctrl Pts',(82.9465924476724,-6.56570339035795,335.709359904124));
#72799=CARTESIAN_POINT('Ctrl Pts',(82.6683544133985,-2.95656296759571,340.905115401276));
#72800=CARTESIAN_POINT('Ctrl Pts',(82.3901163791245,3.36577165173125,340.681833654036));
#72801=CARTESIAN_POINT('Ctrl Pts',(82.1118783448506,6.59938730497258,335.244417026216));
#72802=CARTESIAN_POINT('Ctrl Pts',(81.8336403105766,3.77684263523753,329.582702501026));
#72803=CARTESIAN_POINT('Ctrl Pts',(81.5554022763027,-2.51165477474909,328.892361931465));
#72804=CARTESIAN_POINT('Ctrl Pts',(81.2771642420287,-6.49524366991217,333.806910668809));
#72805=CARTESIAN_POINT('Ctrl Pts',(80.9989262077549,-4.51824331883628,339.816339875417));
#72806=CARTESIAN_POINT('Ctrl Pts',(80.7206881734808,1.6050822367736,341.405885067415));
#72807=CARTESIAN_POINT('Ctrl Pts',(80.442450139207,6.25544751467132,337.116844083755));
#72808=CARTESIAN_POINT('Ctrl Pts',(80.164212104933,5.16528093860915,330.885206529001));
#72809=CARTESIAN_POINT('Ctrl Pts',(79.8859740706591,-0.66498771539297,328.42965420833));
#72810=CARTESIAN_POINT('Ctrl Pts',(79.6077360363851,-5.88500695818154,332.00361124253));
#72811=CARTESIAN_POINT('Ctrl Pts',(79.3294980021113,-5.70444217800723,338.327310012835));
#72812=CARTESIAN_POINT('Ctrl Pts',(79.0512599678372,-0.288995008504218,
341.597585495376));
#72813=CARTESIAN_POINT('Ctrl Pts',(78.7730219335634,5.39165861474379,338.813354149013));
#72814=CARTESIAN_POINT('Ctrl Pts',(78.4947838992893,6.12446670799212,332.529663985116));
#72815=CARTESIAN_POINT('Ctrl Pts',(78.2165458650155,1.23694210029652,328.512964719977));
#72816=CARTESIAN_POINT('Ctrl Pts',(77.9383078307416,-4.78570601560572,330.449321982833));
#72817=CARTESIAN_POINT('Ctrl Pts',(77.6600697964675,-6.41658235789159,336.561769294144));
#72818=CARTESIAN_POINT('Ctrl Pts',(77.3818317621937,-2.1590557789407,341.241003975897));
#72819=CARTESIAN_POINT('Ctrl Pts',(77.1035937279197,4.07980442073289,340.192961426037));
#72820=CARTESIAN_POINT('Ctrl Pts',(76.8253556936458,6.57468832131455,334.379414823488));
#72821=CARTESIAN_POINT('Ctrl Pts',(76.5471176593719,3.03607779166665,329.135370077603));
#72822=CARTESIAN_POINT('Ctrl Pts',(76.2688796250979,-3.28869651495906,329.273209649705));
#72823=CARTESIAN_POINT('Ctrl Pts',(75.990641590824,-6.59548257088784,334.666440198987));
#72824=CARTESIAN_POINT('Ctrl Pts',(75.7124035565499,-3.849691620676,340.365773654324));
#72825=CARTESIAN_POINT('Ctrl Pts',(75.4341655222762,2.428904508475,341.141015825777));
#72826=CARTESIAN_POINT('Ctrl Pts',(75.155927488002,6.47853082077028,336.280738415161));
#72827=CARTESIAN_POINT('Ctrl Pts',(74.8776894537284,4.58290502180284,330.245146264618));
#72828=CARTESIAN_POINT('Ctrl Pts',(74.5994514194541,-1.51838507210583,328.573013205511));
#72829=CARTESIAN_POINT('Ctrl Pts',(74.3212133851804,-6.22627559666991,332.798831065535));
#72830=CARTESIAN_POINT('Ctrl Pts',(74.0429753509063,-5.22040490584718,339.044629167519));
#72831=CARTESIAN_POINT('Ctrl Pts',(73.7647373166325,0.576154314021396,341.578730781099));
#72832=CARTESIAN_POINT('Ctrl Pts',(73.4864992823585,5.84398522393628,338.075628258771));
#72833=CARTESIAN_POINT('Ctrl Pts',(73.2082612480845,5.74887715092534,331.750067079568));
#72834=CARTESIAN_POINT('Ctrl Pts',(72.9300232138107,0.378109369797882,328.406921372514));
#72835=CARTESIAN_POINT('Ctrl Pts',(72.6517851795367,-5.33964379910795,331.114146608223));
#72836=CARTESIAN_POINT('Ctrl Pts',(72.3735471452627,-6.1572846665857,337.387362146464));
#72837=CARTESIAN_POINT('Ctrl Pts',(72.0953091109889,-1.32447627691046,341.469730680301));
#72838=CARTESIAN_POINT('Ctrl Pts',(71.8170710767148,4.72378444284771,339.614922861896));
#72839=CARTESIAN_POINT('Ctrl Pts',(71.5388330424411,6.43709790234862,333.525068449278));
#72840=CARTESIAN_POINT('Ctrl Pts',(71.2605950081669,2.24318162827351,328.788736950804));
#72841=CARTESIAN_POINT('Ctrl Pts',(70.9823569738931,-4.00926931676166,329.752389874485));
#72842=CARTESIAN_POINT('Ctrl Pts',(70.7041189396191,-6.58247298652274,335.531697155753));
#72843=CARTESIAN_POINT('Ctrl Pts',(70.4258809053453,-3.11503835369394,340.823073805024));
#72844=CARTESIAN_POINT('Ctrl Pts',(70.1476428710712,3.21102099842906,340.770701571853));
#72845=CARTESIAN_POINT('Ctrl Pts',(69.8694048367974,6.59037377488596,335.422641681609));
#72846=CARTESIAN_POINT('Ctrl Pts',(69.5911668025233,3.92183781188753,329.686729758333));
#72847=CARTESIAN_POINT('Ctrl Pts',(69.3129287682495,-2.34571082484865,328.826727512095));
#72848=CARTESIAN_POINT('Ctrl Pts',(69.0346907339755,-6.46063526025642,333.631846310655));
#72849=CARTESIAN_POINT('Ctrl Pts',(68.7564526997015,-4.64673007614707,339.692499556012));
#72850=CARTESIAN_POINT('Ctrl Pts',(68.4782146654277,1.43141071321893,341.446915219996));
#72851=CARTESIAN_POINT('Ctrl Pts',(68.1999766311536,6.19596701865144,337.285091942903));
#72852=CARTESIAN_POINT('Ctrl Pts',(67.9217385968798,5.27457584339078,331.026273517709));
#72853=CARTESIAN_POINT('Ctrl Pts',(67.6435005626058,-0.487215730737746,
328.414085233207));
#72854=CARTESIAN_POINT('Ctrl Pts',(67.3652625283319,-5.80189662006064,331.845693722248));
#72855=CARTESIAN_POINT('Ctrl Pts',(67.0870244940579,-5.79226261700764,338.171962524897));
#72856=CARTESIAN_POINT('Ctrl Pts',(66.808786459784,-0.467154703982791,341.587368136539));
#72857=CARTESIAN_POINT('Ctrl Pts',(66.5305484255101,5.28665418569491,338.957643238672));
#72858=CARTESIAN_POINT('Ctrl Pts',(66.2523103912362,6.18897856004828,332.696047555395));
#72859=CARTESIAN_POINT('Ctrl Pts',(65.9740723569621,1.41176865901914,328.548755024249));
#72860=CARTESIAN_POINT('Ctrl Pts',(65.6958343226883,-4.66100050272061,330.32167478713));
#72861=CARTESIAN_POINT('Ctrl Pts',(65.4175962884143,-6.45643829936832,336.387824545895));
#72862=CARTESIAN_POINT('Ctrl Pts',(65.1393582541404,-2.32689796555879,341.180388203148));
#72863=CARTESIAN_POINT('Ctrl Pts',(64.8611202198664,3.93800228628635,340.301300828754));
#72864=CARTESIAN_POINT('Ctrl Pts',(64.5828821855925,6.58905596482498,334.557287930882));
#72865=CARTESIAN_POINT('Ctrl Pts',(64.3046441513185,3.19343023875035,329.219545364423));
#72866=CARTESIAN_POINT('Ctrl Pts',(64.0264061170447,-3.13275928247242,329.18644069766));
#72867=CARTESIAN_POINT('Ctrl Pts',(63.7481680827706,-6.58406184962146,334.488353594661));
#72868=CARTESIAN_POINT('Ctrl Pts',(63.4699300484969,-3.99326803796649,340.259796845953));
#72869=CARTESIAN_POINT('Ctrl Pts',(63.1916920142227,2.2620889115907,341.204402166188));
#72870=CARTESIAN_POINT('Ctrl Pts',(62.9134539799489,6.44156025535872,336.455319195338));
#72871=CARTESIAN_POINT('Ctrl Pts',(62.6352159456749,4.70970683005755,330.370711279404));
#72872=CARTESIAN_POINT('Ctrl Pts',(62.356977911401,-1.34417503802856,328.53433329417));
#72873=CARTESIAN_POINT('Ctrl Pts',(62.0787398771271,-6.16452731370681,332.631402211794));
#72874=CARTESIAN_POINT('Ctrl Pts',(61.8005018428531,-5.32778386187053,338.902098359207));
#72875=CARTESIAN_POINT('Ctrl Pts',(61.5222638085792,0.39818820204327,341.591896437255));
#72876=CARTESIAN_POINT('Ctrl Pts',(61.2440257743053,5.75874883019031,338.232408451065));
#72877=CARTESIAN_POINT('Ctrl Pts',(60.9657877400313,5.8345906558651,331.906586939604));
#72878=CARTESIAN_POINT('Ctrl Pts',(60.6875497057574,0.556114755069404,328.419544934966));
#72879=CARTESIAN_POINT('Ctrl Pts',(60.4093116714834,-5.23269944821315,330.971289416152));
#72880=CARTESIAN_POINT('Ctrl Pts',(60.1310736372095,-6.21954260238776,337.220122136465));
#72881=CARTESIAN_POINT('Ctrl Pts',(59.8528356029356,-1.49880331064944,341.431581541093));
#72882=CARTESIAN_POINT('Ctrl Pts',(59.5745975686616,4.59736565697126,339.740873495448));
#72883=CARTESIAN_POINT('Ctrl Pts',(59.2963595343877,6.47460001819531,333.699535818209));
#72884=CARTESIAN_POINT('Ctrl Pts',(59.0181215001138,2.41018950766113,328.85161492578));
#72885=CARTESIAN_POINT('Ctrl Pts',(58.7398834658397,-3.86601633971484,329.645976265948));
#72886=CARTESIAN_POINT('Ctrl Pts',(58.461645431566,-6.59443605444214,335.353646161595));
#72887=CARTESIAN_POINT('Ctrl Pts',(58.1834073972918,-3.27123913572451,340.736780194555));
#72888=CARTESIAN_POINT('Ctrl Pts',(57.9051693630181,3.05392565443701,340.855355717709));
#72889=CARTESIAN_POINT('Ctrl Pts',(57.626931328744,6.57654794739045,335.60055772363));
#72890=CARTESIAN_POINT('Ctrl Pts',(57.3486932944702,4.06396925871226,329.794636770793));
#72891=CARTESIAN_POINT('Ctrl Pts',(57.0704552601961,-2.17805403459824,328.765600822364));
#72892=CARTESIAN_POINT('Ctrl Pts',(56.7922172259222,-6.42130928838279,333.457780979671));
#72893=CARTESIAN_POINT('Ctrl Pts',(56.5139791916483,-4.7718237865882,339.565232768818));
#72894=CARTESIAN_POINT('Ctrl Pts',(56.2357411573743,1.25669397215475,341.483237828746));
#72895=CARTESIAN_POINT('Ctrl Pts',(55.9575031231004,6.13196222142391,337.451671225668));
#72896=CARTESIAN_POINT('Ctrl Pts',(55.6792650888265,5.38001924770637,331.170242125401));
#72897=CARTESIAN_POINT('Ctrl Pts',(55.4010270545525,-0.309087980677374,
328.403325299521));
#72898=CARTESIAN_POINT('Ctrl Pts',(55.1227890202786,-5.7145497313246,331.690079479511));
#72899=CARTESIAN_POINT('Ctrl Pts',(54.8445509860047,-5.87585354015102,338.014298866807));
#72900=CARTESIAN_POINT('Ctrl Pts',(54.5663129517307,-0.644973282637039,
341.572340675012));
#72901=CARTESIAN_POINT('Ctrl Pts',(54.2880749174568,5.17778943656281,339.099042453349));
#72902=CARTESIAN_POINT('Ctrl Pts',(54.0098368831829,6.24897121387603,332.864113474015));
#72903=CARTESIAN_POINT('Ctrl Pts',(53.7315988489089,1.58556434287916,328.589256033944));
#72904=CARTESIAN_POINT('Ctrl Pts',(53.453360814635,-4.53289152268657,330.197443709097));
#72905=CARTESIAN_POINT('Ctrl Pts',(53.175122780361,-6.49157974325204,336.212866406798));
#72906=CARTESIAN_POINT('Ctrl Pts',(52.8968847460871,-2.49304104899505,341.115259504858));
#72907=CARTESIAN_POINT('Ctrl Pts',(52.6186467118132,3.79332461869913,340.405769216394));
#72908=CARTESIAN_POINT('Ctrl Pts',(52.3404086775392,6.59861227319271,334.735484307067));
#72909=CARTESIAN_POINT('Ctrl Pts',(52.0621706432654,3.34845083993485,329.307941544899));
#72910=CARTESIAN_POINT('Ctrl Pts',(51.7839326089913,-2.97453450607784,329.103916812333));
#72911=CARTESIAN_POINT('Ctrl Pts',(51.5056945747175,-6.56783343992024,334.310640595043));
#72912=CARTESIAN_POINT('Ctrl Pts',(51.2274565404434,-4.13392856701051,340.149979328754));
#72913=CARTESIAN_POINT('Ctrl Pts',(50.9492185061695,2.09362153515914,341.263258046037));
#72914=CARTESIAN_POINT('Ctrl Pts',(50.6709804718956,6.39988605631644,336.62883730001));
#72915=CARTESIAN_POINT('Ctrl Pts',(50.3927424376217,4.8330696057555,330.499656605363));
#72916=CARTESIAN_POINT('Ctrl Pts',(50.1145044033477,-1.16898348601682,328.500374619014));
#72917=CARTESIAN_POINT('Ctrl Pts',(49.8362663690738,-6.09827768683947,332.465702910484));
#72918=CARTESIAN_POINT('Ctrl Pts',(49.5580283347998,-5.43127246488066,338.756718234838));
#72919=CARTESIAN_POINT('Ctrl Pts',(49.279790300526,0.21993133264897,341.600248684153));
#72920=CARTESIAN_POINT('Ctrl Pts',(49.0015522662519,5.66930739238778,338.386828335532));
#72921=CARTESIAN_POINT('Ctrl Pts',(48.7233142319781,5.91604373697227,332.065365612896));
#72922=CARTESIAN_POINT('Ctrl Pts',(48.445076197704,0.73371406479973,328.436973552176));
#72923=CARTESIAN_POINT('Ctrl Pts',(48.1668381634302,-5.12193417503768,330.83137399251));
#72924=CARTESIAN_POINT('Ctrl Pts',(47.8886001291562,-6.27725902206752,337.051260991101));
#72925=CARTESIAN_POINT('Ctrl Pts',(47.6103620948823,-1.67203591673728,341.388736054719));
#72926=CARTESIAN_POINT('Ctrl Pts',(47.3321240606083,4.46758987017308,339.863362338513));
#72927=CARTESIAN_POINT('Ctrl Pts',(47.0538860263344,6.50737437474395,333.874952787363));
#72928=CARTESIAN_POINT('Ctrl Pts',(46.7756479920604,2.57543746430089,328.918982457581));
#72929=CARTESIAN_POINT('Ctrl Pts',(46.4974099577865,-3.71994039373653,329.543472170804));
#72930=CARTESIAN_POINT('Ctrl Pts',(46.2191719235126,-6.6015838586722,335.175336934662));
#72931=CARTESIAN_POINT('Ctrl Pts',(45.9409338892386,-3.42505125572216,340.64629758155));
#72932=CARTESIAN_POINT('Ctrl Pts',(45.6626958549647,2.89460033093036,340.935734277064));
#72933=CARTESIAN_POINT('Ctrl Pts',(45.3844578206908,6.55791991811895,335.778035237812));
#72934=CARTESIAN_POINT('Ctrl Pts',(45.1062197864168,4.2031331911891,329.9063447446));
#72935=CARTESIAN_POINT('Ctrl Pts',(44.8279817521429,-2.00880682715078,328.709026497041));
#72936=CARTESIAN_POINT('Ctrl Pts',(44.5497437178689,-6.37729447015455,333.284841778531));
#72937=CARTESIAN_POINT('Ctrl Pts',(44.2715056835951,-4.89343310660957,339.434632444168));
#72938=CARTESIAN_POINT('Ctrl Pts',(43.993267649321,1.08105959191674,341.514826370861));
#72939=CARTESIAN_POINT('Ctrl Pts',(43.7150296150472,6.06347985935449,337.616460295694));
#72940=CARTESIAN_POINT('Ctrl Pts',(43.4367915807731,5.48153415667863,331.317007226059));
#72941=CARTESIAN_POINT('Ctrl Pts',(43.1585535464993,-0.130734534269442,
328.397382264187));
#72942=CARTESIAN_POINT('Ctrl Pts',(42.8803155122253,-5.62303007275688,331.536882143992));
#72943=CARTESIAN_POINT('Ctrl Pts',(42.6020774779514,-5.95515390926368,337.854434164719));
#72944=CARTESIAN_POINT('Ctrl Pts',(42.3238394436775,-0.822320901166817,
341.552514083865));
#72945=CARTESIAN_POINT('Ctrl Pts',(42.0456014094035,5.06514386049422,339.237448543196));
#72946=CARTESIAN_POINT('Ctrl Pts',(41.7673633751296,6.30440086278054,333.033739019075));
#72947=CARTESIAN_POINT('Ctrl Pts',(41.4891253408556,1.75820224609737,328.634438175184));
#72948=CARTESIAN_POINT('Ctrl Pts',(41.2108873065818,-4.40147262080676,330.076719462388));
#72949=CARTESIAN_POINT('Ctrl Pts',(40.9326492723077,-6.5219810292259,336.037022631457));
#72950=CARTESIAN_POINT('Ctrl Pts',(40.6544112380339,-2.65736371140664,341.045665438067));
#72951=CARTESIAN_POINT('Ctrl Pts',(40.3761732037599,3.64587706174641,340.506290306038));
#72952=CARTESIAN_POINT('Ctrl Pts',(40.097935169486,6.603350268392,334.91387383287));
#72953=CARTESIAN_POINT('Ctrl Pts',(39.819697135212,3.50102639902445,329.400494072056));
#72954=CARTESIAN_POINT('Ctrl Pts',(39.5414591009381,-2.8141377216629,329.025698252745));
#72955=CARTESIAN_POINT('Ctrl Pts',(39.2632210666642,-6.54680919178488,334.13343096634));
#72956=CARTESIAN_POINT('Ctrl Pts',(38.9849830323901,-4.27157049735116,340.036401291587));
#72957=CARTESIAN_POINT('Ctrl Pts',(38.7067449981163,1.92362539422454,341.317540488706));
#72958=CARTESIAN_POINT('Ctrl Pts',(38.4285069638423,6.35353865418465,336.801166026084));
#72959=CARTESIAN_POINT('Ctrl Pts',(38.1502689295684,4.95290326927633,330.631888086492));
#72960=CARTESIAN_POINT('Ctrl Pts',(37.8720308952944,-0.99293834111446,328.471161976701));
#72961=CARTESIAN_POINT('Ctrl Pts',(37.5937928610205,-6.0275750916104,332.301854155399));
#72962=CARTESIAN_POINT('Ctrl Pts',(37.3155548267466,-5.530795147398,338.608594951121));
#72963=CARTESIAN_POINT('Ctrl Pts',(37.0373167924726,0.0415138691789895,
341.603781422973));
#72964=CARTESIAN_POINT('Ctrl Pts',(36.7590787581987,5.57572622075412,338.538775154617));
#72965=CARTESIAN_POINT('Ctrl Pts',(36.4808407239247,5.99317691712731,332.226287159104));
#72966=CARTESIAN_POINT('Ctrl Pts',(36.2026026896508,0.910777615799064,328.459194497748));
#72967=CARTESIAN_POINT('Ctrl Pts',(35.9243646553769,-5.00742886049242,330.694502503677));
#72968=CARTESIAN_POINT('Ctrl Pts',(35.646126621103,-6.33039178103882,336.880902012943));
#72969=CARTESIAN_POINT('Ctrl Pts',(35.367888586829,-1.84404760055544,341.341225507));
#72970=CARTESIAN_POINT('Ctrl Pts',(35.0896505525551,4.3345518448597,339.982299949618));
#72971=CARTESIAN_POINT('Ctrl Pts',(34.8114125182811,6.53539704012746,334.051191267098));
#72972=CARTESIAN_POINT('Ctrl Pts',(34.5331744840072,2.73880483397243,328.990790354369));
#72973=CARTESIAN_POINT('Ctrl Pts',(34.2549364497332,-3.571148143626,329.444952437646));
#72974=CARTESIAN_POINT('Ctrl Pts',(33.9766984154593,-6.60391117987907,334.996899676528));
#72975=CARTESIAN_POINT('Ctrl Pts',(33.6984603811854,-3.57636239992634,340.5516920365));
#72976=CARTESIAN_POINT('Ctrl Pts',(33.4202223469114,2.73316136741629,341.011778557416));
#72977=CARTESIAN_POINT('Ctrl Pts',(33.1419843126375,6.53450328927665,335.954944629898));
#72978=CARTESIAN_POINT('Ctrl Pts',(32.8637462783636,4.33922799167826,330.021772110482));
#72979=CARTESIAN_POINT('Ctrl Pts',(32.5855082440896,-1.83809278698308,328.657045846753));
#72980=CARTESIAN_POINT('Ctrl Pts',(32.3072702098157,-6.32862294523512,333.113154987611));
#72981=CARTESIAN_POINT('Ctrl Pts',(32.0290321755417,-5.01146923696644,339.300793946549));
#72982=CARTESIAN_POINT('Ctrl Pts',(31.7507941412678,0.904635820901655,341.541657780355));
#72983=CARTESIAN_POINT('Ctrl Pts',(31.4725561069938,5.99056993833113,337.779338823839));
#72984=CARTESIAN_POINT('Ctrl Pts',(31.19431807272,5.57904644402149,331.46646165166));
#72985=CARTESIAN_POINT('Ctrl Pts',(30.9160800384459,0.047714374623849,328.396260466811));
#72986=CARTESIAN_POINT('Ctrl Pts',(30.6378420041721,-5.52740447210307,331.386213580536));
#72987=CARTESIAN_POINT('Ctrl Pts',(30.359603969898,-6.03010581913728,337.692485152001));
#72988=CARTESIAN_POINT('Ctrl Pts',(30.0813659356242,-0.999068060165199,
341.527902840492));
#72989=CARTESIAN_POINT('Ctrl Pts',(29.8031279013501,4.94879971140008,339.372760443951));
#72990=CARTESIAN_POINT('Ctrl Pts',(29.5248898670764,6.35522703197753,333.204800329835));
#72991=CARTESIAN_POINT('Ctrl Pts',(29.2466518328023,1.92955630830642,328.684268455926));
#72992=CARTESIAN_POINT('Ctrl Pts',(28.9684137985284,-4.26683975929307,329.959590199969));
#72993=CARTESIAN_POINT('Ctrl Pts',(28.6901757642544,-6.54761995824091,335.860421621174));
#72994=CARTESIAN_POINT('Ctrl Pts',(28.4119377299806,-2.81974596422338,340.971656820429));
#72995=CARTESIAN_POINT('Ctrl Pts',(28.1336996957066,3.49576728177937,340.602790697088));
#72996=CARTESIAN_POINT('Ctrl Pts',(27.8554616614327,6.60326649073411,335.092326248084));
#72997=CARTESIAN_POINT('Ctrl Pts',(27.5772236271588,3.6510455051959,329.497135363947));
#72998=CARTESIAN_POINT('Ctrl Pts',(27.2989855928848,-2.65168605111725,328.951842134166));
#72999=CARTESIAN_POINT('Ctrl Pts',(27.0207475586109,-6.52100445714207,333.956854107198));
#73000=CARTESIAN_POINT('Ctrl Pts',(26.7425095243369,-4.40609332271562,339.919145669246));
#73001=CARTESIAN_POINT('Ctrl Pts',(26.464271490063,1.75222462013611,341.367209857098));
#73002=CARTESIAN_POINT('Ctrl Pts',(26.1860334557891,6.30255189188194,336.972179538955));
#73003=CARTESIAN_POINT('Ctrl Pts',(25.9077954215151,5.06912031796114,330.767309167235));
#73004=CARTESIAN_POINT('Ctrl Pts',(25.6295573872412,-0.816168151659336,
328.446716698329));
#73005=CARTESIAN_POINT('Ctrl Pts',(25.3513193529672,-5.95247115512422,332.139975589065));
#73006=CARTESIAN_POINT('Ctrl Pts',(25.0730813186933,-5.62627923786184,338.457836667822));
#73007=CARTESIAN_POINT('Ctrl Pts',(24.7948432844193,-0.136933907759072,
341.602492074107));
#73008=CARTESIAN_POINT('Ctrl Pts',(24.5166052501454,5.47807364835303,338.688137956606));
#73009=CARTESIAN_POINT('Ctrl Pts',(24.2383672158715,6.06593387360606,332.389234073155));
#73010=CARTESIAN_POINT('Ctrl Pts',(23.9601291815975,1.08717611608803,328.486191545927));
#73011=CARTESIAN_POINT('Ctrl Pts',(23.6818911473236,-4.88926711647082,330.560774893348));
#73012=CARTESIAN_POINT('Ctrl Pts',(23.4036531130496,-6.37890208170874,336.709169598286));
#73013=CARTESIAN_POINT('Ctrl Pts',(23.1254150787758,-2.01471275900294,341.289084590182));
#73014=CARTESIAN_POINT('Ctrl Pts',(22.8471770445018,4.19834872552828,340.097599480402));
#73015=CARTESIAN_POINT('Ctrl Pts',(22.5689390102279,6.55864755216782,334.228122567904));
#73016=CARTESIAN_POINT('Ctrl Pts',(22.2907009759539,2.90017232566213,329.066986181947));
#73017=CARTESIAN_POINT('Ctrl Pts',(22.01246294168,-3.41974823763033,329.350489005678));
#73018=CARTESIAN_POINT('Ctrl Pts',(21.734224907406,-6.60141631865069,334.818464682252));
#73019=CARTESIAN_POINT('Ctrl Pts',(21.4559868731321,-3.72506208079045,340.453032640467));
#73020=CARTESIAN_POINT('Ctrl Pts',(21.1777488388582,2.56972664678499,341.083433031154));
#73021=CARTESIAN_POINT('Ctrl Pts',(20.8995108045842,6.50631515970899,336.131156720477));
#73022=CARTESIAN_POINT('Ctrl Pts',(20.6212727703103,4.47215428362238,330.140834583263));
#73023=CARTESIAN_POINT('Ctrl Pts',(20.3430347360363,-1.66603656965545,328.609696827826));
#73024=CARTESIAN_POINT('Ctrl Pts',(20.0647967017624,-6.27533025361995,332.942845972772));
#73025=CARTESIAN_POINT('Ctrl Pts',(19.7865586674884,-5.12584598756012,339.163815004963));
#73026=CARTESIAN_POINT('Ctrl Pts',(19.5083206332146,0.727551483920866,341.563712464907));
#73027=CARTESIAN_POINT('Ctrl Pts',(19.2300825989406,5.91328569724997,337.940187876045));
#73028=CARTESIAN_POINT('Ctrl Pts',(18.9518445646666,5.6724849061666,331.618496270436));
#73029=CARTESIAN_POINT('Ctrl Pts',(18.6736065303927,0.226128442434109,328.399960726537));
#73030=CARTESIAN_POINT('Ctrl Pts',(18.3953684961188,-5.42774275526982,331.238183807473));
#73031=CARTESIAN_POINT('Ctrl Pts',(18.1171304618448,-6.10065453981439,337.528570083977));
#73032=CARTESIAN_POINT('Ctrl Pts',(17.8388924275709,-1.17508569868469,341.498524916047));
#73033=CARTESIAN_POINT('Ctrl Pts',(17.560654393297,4.82884194389145,339.504879350732));
#73034=CARTESIAN_POINT('Ctrl Pts',(17.282416359023,6.4014126081487,333.377172497161));
#73035=CARTESIAN_POINT('Ctrl Pts',(17.0041783247491,2.09950140660303,328.73871049005));
#73036=CARTESIAN_POINT('Ctrl Pts',(16.7259402904752,-4.12909124719214,329.846141449739));
#73037=CARTESIAN_POINT('Ctrl Pts',(16.4477022562012,-6.56847780872623,335.683192330176));
#73038=CARTESIAN_POINT('Ctrl Pts',(16.1694642219273,-2.98006923576536,340.893287693111));
#73039=CARTESIAN_POINT('Ctrl Pts',(15.8912261876533,3.34310488910675,340.695199924864));
#73040=CARTESIAN_POINT('Ctrl Pts',(15.6129881533794,6.59836100139441,335.270711246581));
#73041=CARTESIAN_POINT('Ctrl Pts',(15.3347501191054,3.79839861434825,329.597794853003));
#73042=CARTESIAN_POINT('Ctrl Pts',(15.0565120848315,-2.48729811680818,328.882402386407));
#73043=CARTESIAN_POINT('Ctrl Pts',(14.7782740505576,-6.49043807864009,333.781038954212));
#73044=CARTESIAN_POINT('Ctrl Pts',(14.5000360162836,-4.5373988143935,339.798298081903));
#73045=CARTESIAN_POINT('Ctrl Pts',(14.2217979820097,1.57954436988845,341.412229882592));
#73046=CARTESIAN_POINT('Ctrl Pts',(13.9435599477357,6.24696300003001,337.141752964392));
#73047=CARTESIAN_POINT('Ctrl Pts',(13.6653219134619,5.18163588993546,330.905820962976));
#73048=CARTESIAN_POINT('Ctrl Pts',(13.3870838791879,-0.638801995284358,
328.427056633885));
#73049=CARTESIAN_POINT('Ctrl Pts',(13.108845844914,-5.87302071860168,331.980185415332));
#73050=CARTESIAN_POINT('Ctrl Pts',(12.83060781064,-5.71765501321869,338.304553468852));
#73051=CARTESIAN_POINT('Ctrl Pts',(12.5523697763661,-0.315281696323335,
341.596381578923));
#73052=CARTESIAN_POINT('Ctrl Pts',(12.2741317420922,5.37642098288874,338.83480767685));
#73053=CARTESIAN_POINT('Ctrl Pts',(11.9958937078182,6.13426147599768,332.554087370642));
#73054=CARTESIAN_POINT('Ctrl Pts',(11.7176556735443,1.26278076536891,328.517944984216));
#73055=CARTESIAN_POINT('Ctrl Pts',(11.4394176392703,-4.76753523623819,330.430288808096));
#73056=CARTESIAN_POINT('Ctrl Pts',(11.1611796049964,-6.4227544802001,336.536189149064));
#73057=CARTESIAN_POINT('Ctrl Pts',(10.8829415707225,-2.18390681301347,341.232351372412));
#73058=CARTESIAN_POINT('Ctrl Pts',(10.6047035364485,4.05908004486941,340.209176748852));
#73059=CARTESIAN_POINT('Ctrl Pts',(10.3264655021746,6.57710878785304,334.405617475831));
#73060=CARTESIAN_POINT('Ctrl Pts',(10.0482274679006,3.05942238333672,329.147514337048));
#73061=CARTESIAN_POINT('Ctrl Pts',(9.76998943362672,-3.26585174673895,329.260150786106));
#73062=CARTESIAN_POINT('Ctrl Pts',(9.49175139935276,-6.59410011745994,334.640162370028));
#73063=CARTESIAN_POINT('Ctrl Pts',(9.21351336507884,-3.87104356673585,340.350391199024));
#73064=CARTESIAN_POINT('Ctrl Pts',(8.9352753308049,2.4044190006588,341.150645821003));
#73065=CARTESIAN_POINT('Ctrl Pts',(8.65703729653096,6.47336951988847,336.306541999263));
#73066=CARTESIAN_POINT('Ctrl Pts',(8.37879926225703,4.60182745214506,330.263446809577));
#73067=CARTESIAN_POINT('Ctrl Pts',(8.10056122798305,-1.49278731520583,328.567011019545));
#73068=CARTESIAN_POINT('Ctrl Pts',(7.82232319370917,-6.21741092854858,332.774044749012));
#73069=CARTESIAN_POINT('Ctrl Pts',(7.54408515943517,-5.23656364109403,339.023784963449));
#73070=CARTESIAN_POINT('Ctrl Pts',(7.2658471251613,0.550094121815325,341.580994482456));
#73071=CARTESIAN_POINT('Ctrl Pts',(6.98760909088731,5.83138478454036,338.098851931026));
#73072=CARTESIAN_POINT('Ctrl Pts',(6.70937105661341,5.7623455394068,331.773071937739));
#73073=CARTESIAN_POINT('Ctrl Pts',(6.43113302233942,0.403311536316757,328.408344724868));
#73074=CARTESIAN_POINT('Ctrl Pts',(6.15289498806554,-5.32210119679797,331.09315624518));
#73075=CARTESIAN_POINT('Ctrl Pts',(5.87465695379156,-6.17058839537894,337.362332615213));
#73076=CARTESIAN_POINT('Ctrl Pts',(5.59641891951763,-1.3427309658529,341.465250565794));
#73077=CARTESIAN_POINT('Ctrl Pts',(5.36455389095603,3.6837204961337,339.938001672926));
#73078=CARTESIAN_POINT('Ctrl Pts',(5.17906186810672,5.59027261763526,336.589093317143));
#73079=CARTESIAN_POINT('Ctrl Pts',(5.08631585668207,5.65257316228901,334.68157454258));
#73080=CARTESIAN_POINT('Ctrl Pts',(5.03994285096975,5.44851606351237,333.774411599427));
#73081=CARTESIAN_POINT('Ctrl Pts',(185.422610796143,3.04869533563088,339.272759684468));
#73082=CARTESIAN_POINT('Ctrl Pts',(185.376227986451,3.76025219667377,338.765053977827));
#73083=CARTESIAN_POINT('Ctrl Pts',(185.283472171046,4.91198743119452,337.389569652041));
#73084=CARTESIAN_POINT('Ctrl Pts',(185.097970344217,5.67465640099036,333.848674163514));
#73085=CARTESIAN_POINT('Ctrl Pts',(184.866105315656,3.1102034485172,329.629352350811));
#73086=CARTESIAN_POINT('Ctrl Pts',(184.587867281381,-2.84276674491428,329.478773562289));
#73087=CARTESIAN_POINT('Ctrl Pts',(184.309629247108,-6.17636874974876,334.402383897492));
#73088=CARTESIAN_POINT('Ctrl Pts',(184.031391212834,-3.84753045006414,339.870598632012));
#73089=CARTESIAN_POINT('Ctrl Pts',(183.75315317856,2.01504287056116,340.871144614342));
#73090=CARTESIAN_POINT('Ctrl Pts',(183.474915144286,6.02689969073261,336.482766363536));
#73091=CARTESIAN_POINT('Ctrl Pts',(183.196677110012,4.50877578226168,330.734237247225));
#73092=CARTESIAN_POINT('Ctrl Pts',(182.918439075738,-1.14741733317675,328.900038067762));
#73093=CARTESIAN_POINT('Ctrl Pts',(182.640201041464,-5.75041359440766,332.663841513818));
#73094=CARTESIAN_POINT('Ctrl Pts',(182.36196300719,-5.07646140385426,338.571419658156));
#73095=CARTESIAN_POINT('Ctrl Pts',(182.083724972916,0.256148691274596,341.201602898475));
#73096=CARTESIAN_POINT('Ctrl Pts',(181.805486938642,5.35366091116605,338.140643284717));
#73097=CARTESIAN_POINT('Ctrl Pts',(181.527248904368,5.53821554038123,332.197574082239));
#73098=CARTESIAN_POINT('Ctrl Pts',(181.249010870094,0.640421975222099,328.826243214803));
#73099=CARTESIAN_POINT('Ctrl Pts',(180.97077283582,-4.84507233320865,331.120481301994));
#73100=CARTESIAN_POINT('Ctrl Pts',(180.692534801546,-5.88431794951573,336.974894595124));
#73101=CARTESIAN_POINT('Ctrl Pts',(180.414296767273,-1.52361041929907,341.016977243033));
#73102=CARTESIAN_POINT('Ctrl Pts',(180.136058732998,4.23529115399526,339.537368168912));
#73103=CARTESIAN_POINT('Ctrl Pts',(179.857820698725,6.10752894540388,333.893883571184));
#73104=CARTESIAN_POINT('Ctrl Pts',(179.579582664451,2.37497736016159,329.265465549051));
#73105=CARTESIAN_POINT('Ctrl Pts',(179.301344630176,-3.53705578244632,329.899545227691));
#73106=CARTESIAN_POINT('Ctrl Pts',(179.023106595903,-6.20318509938342,335.214236927654));
#73107=CARTESIAN_POINT('Ctrl Pts',(178.744868561628,-3.17674297821987,340.332326582762));
#73108=CARTESIAN_POINT('Ctrl Pts',(178.466630527355,2.76494926885195,340.557018826482));
#73109=CARTESIAN_POINT('Ctrl Pts',(178.188392493081,6.16928839125002,335.682116920639));
#73110=CARTESIAN_POINT('Ctrl Pts',(177.910154458807,3.91216261090214,330.181246381558));
#73111=CARTESIAN_POINT('Ctrl Pts',(177.631916424533,-1.93509705158604,329.102474915127));
#73112=CARTESIAN_POINT('Ctrl Pts',(177.353678390259,-6.00654671312173,333.43577517086));
#73113=CARTESIAN_POINT('Ctrl Pts',(177.075440355985,-4.56587711182005,339.204541464849));
#73114=CARTESIAN_POINT('Ctrl Pts',(176.797202321711,1.0648305223979,341.114862115224));
#73115=CARTESIAN_POINT('Ctrl Pts',(176.518964287437,5.71835890327751,337.41366405781));
#73116=CARTESIAN_POINT('Ctrl Pts',(176.240726253163,5.12423372135596,331.497482120095));
#73117=CARTESIAN_POINT('Ctrl Pts',(175.962488218889,-0.172325113033902,
328.795509143729));
#73118=CARTESIAN_POINT('Ctrl Pts',(175.684250184616,-5.31074373473581,331.787305848006));
#73119=CARTESIAN_POINT('Ctrl Pts',(175.406012150341,-5.57557121750448,337.727344556293));
#73120=CARTESIAN_POINT('Ctrl Pts',(175.127774116067,-0.723779289273663,
341.164539420802));
#73121=CARTESIAN_POINT('Ctrl Pts',(174.849536081794,4.79221420976308,338.944627447299));
#73122=CARTESIAN_POINT('Ctrl Pts',(174.571298047519,5.91046346146377,333.104789088012));
#73123=CARTESIAN_POINT('Ctrl Pts',(174.293060013246,1.6047676328781,329.004157809391));
#73124=CARTESIAN_POINT('Ctrl Pts',(174.014821978972,-4.17359976606904,330.405822410606));
#73125=CARTESIAN_POINT('Ctrl Pts',(173.736583944698,-6.12191626192584,336.023495975658));
#73126=CARTESIAN_POINT('Ctrl Pts',(173.458345910424,-2.45224056354941,340.701922390625));
#73127=CARTESIAN_POINT('Ctrl Pts',(173.18010787615,3.467820104985,340.147778787951));
#73128=CARTESIAN_POINT('Ctrl Pts',(172.901869841876,6.20551344811549,334.869594572666));
#73129=CARTESIAN_POINT('Ctrl Pts',(172.623631807602,3.24849869313879,329.711081493264));
#73130=CARTESIAN_POINT('Ctrl Pts',(172.345393773329,-2.68961536476926,329.406130863184));
#73131=CARTESIAN_POINT('Ctrl Pts',(172.067155739054,-6.15950910108628,334.234591374587));
#73132=CARTESIAN_POINT('Ctrl Pts',(171.788917704781,-3.97691224954176,339.76545608412));
#73133=CARTESIAN_POINT('Ctrl Pts',(171.510679670506,1.85523827427864,340.923132083271));
#73134=CARTESIAN_POINT('Ctrl Pts',(171.232441636233,5.98486401706558,336.645237194892));
#73135=CARTESIAN_POINT('Ctrl Pts',(170.954203601958,4.62226838783954,330.857532416421));
#73136=CARTESIAN_POINT('Ctrl Pts',(170.675965567685,-0.982114716337224,
328.87130899668));
#73137=CARTESIAN_POINT('Ctrl Pts',(170.397727533411,-5.6852256413208,332.509294851355));
#73138=CARTESIAN_POINT('Ctrl Pts',(170.119489499137,-5.17108890905721,338.432964058193));
#73139=CARTESIAN_POINT('Ctrl Pts',(169.841251464863,0.0884797899009875,
341.206252819294));
#73140=CARTESIAN_POINT('Ctrl Pts',(169.563013430589,5.26685189162661,338.284154972271));
#73141=CARTESIAN_POINT('Ctrl Pts',(169.284775396315,5.61191175101298,332.348236581241));
#73142=CARTESIAN_POINT('Ctrl Pts',(169.006537362041,0.807003028176409,328.845802339644));
#73143=CARTESIAN_POINT('Ctrl Pts',(168.728299327767,-4.73848046227249,330.990984455146));
#73144=CARTESIAN_POINT('Ctrl Pts',(168.450061293493,-5.93553037235089,336.815180963188));
#73145=CARTESIAN_POINT('Ctrl Pts',(168.171823259219,-1.6856316680076,340.97361269334));
#73146=CARTESIAN_POINT('Ctrl Pts',(167.893585224945,4.11114633818361,339.650148225192));
#73147=CARTESIAN_POINT('Ctrl Pts',(167.615347190671,6.13518603024423,334.059311366861));
#73148=CARTESIAN_POINT('Ctrl Pts',(167.337109156397,2.52905605754718,329.33173058262));
#73149=CARTESIAN_POINT('Ctrl Pts',(167.058871122123,-3.3979513303547,329.805836979189));
#73150=CARTESIAN_POINT('Ctrl Pts',(166.780633087849,-6.20670893606953,335.046550114236));
#73151=CARTESIAN_POINT('Ctrl Pts',(166.502395053576,-3.31966136202707,340.244544896527));
#73152=CARTESIAN_POINT('Ctrl Pts',(166.224157019301,2.61379044582624,340.629698236632));
#73153=CARTESIAN_POINT('Ctrl Pts',(165.945918985028,6.14860534102855,335.848560599189));
#73154=CARTESIAN_POINT('Ctrl Pts',(165.667680950753,4.04093586803504,330.288711424605));
#73155=CARTESIAN_POINT('Ctrl Pts',(165.38944291648,-1.77504080693859,329.052342237156));
#73156=CARTESIAN_POINT('Ctrl Pts',(165.111204882206,-5.96208873294403,333.274050791383));
#73157=CARTESIAN_POINT('Ctrl Pts',(164.832966847932,-4.67781582901218,339.079637459391));
#73158=CARTESIAN_POINT('Ctrl Pts',(164.554728813658,0.899219616755684,341.141401046264));
#73159=CARTESIAN_POINT('Ctrl Pts',(164.276490779384,5.65105449268665,337.567291539913));
#73160=CARTESIAN_POINT('Ctrl Pts',(163.99825274511,5.21700007010667,331.637216480543));
#73161=CARTESIAN_POINT('Ctrl Pts',(163.720014710836,-0.00461831401527035,
328.793118222377));
#73162=CARTESIAN_POINT('Ctrl Pts',(163.441776676562,-5.22199853953164,331.644983758109));
#73163=CARTESIAN_POINT('Ctrl Pts',(163.163538642288,-5.64722778189197,337.575698179067));
#73164=CARTESIAN_POINT('Ctrl Pts',(162.885300608014,-0.89007944175547,341.142732398337));
#73165=CARTESIAN_POINT('Ctrl Pts',(162.60706257374,4.68388166452899,339.072671762236));
#73166=CARTESIAN_POINT('Ctrl Pts',(162.328824539466,5.95951370125524,333.265180362466));
#73167=CARTESIAN_POINT('Ctrl Pts',(162.050586505192,1.7661879766176,329.049707338167));
#73168=CARTESIAN_POINT('Ctrl Pts',(161.772348470919,-4.04794238527021,330.294730063455));
#73169=CARTESIAN_POINT('Ctrl Pts',(161.494110436645,-6.14733576772723,335.857709559841));
#73170=CARTESIAN_POINT('Ctrl Pts',(161.215872402371,-2.60540985066816,340.633581652932));
#73171=CARTESIAN_POINT('Ctrl Pts',(160.937634368097,3.32746223056271,340.239599014658));
#73172=CARTESIAN_POINT('Ctrl Pts',(160.659396333823,6.20677133606821,335.037313696985));
#73173=CARTESIAN_POINT('Ctrl Pts',(160.381158299549,3.39021799825867,329.800786150339));
#73174=CARTESIAN_POINT('Ctrl Pts',(160.102920265275,-2.53748835701711,329.335500413256));
#73175=CARTESIAN_POINT('Ctrl Pts',(159.824682231001,-6.13657910032513,334.068442339051));
#73176=CARTESIAN_POINT('Ctrl Pts',(159.546444196727,-4.10422177902387,339.65626098053));
#73177=CARTESIAN_POINT('Ctrl Pts',(159.268206162453,1.69451929067344,340.971097646477));
#73178=CARTESIAN_POINT('Ctrl Pts',(158.989968128179,5.93822501838346,336.806346135508));
#73179=CARTESIAN_POINT('Ctrl Pts',(158.711730093905,4.73250929478059,330.983937437609));
#73180=CARTESIAN_POINT('Ctrl Pts',(158.433492059631,-0.816160356919756,
328.84701007623));
#73181=CARTESIAN_POINT('Ctrl Pts',(158.155254025357,-5.61585169558195,332.356590749912));
#73182=CARTESIAN_POINT('Ctrl Pts',(157.877015991083,-5.26195882304375,338.291989075743));
#73183=CARTESIAN_POINT('Ctrl Pts',(157.598777956809,-0.0792440049832126,
341.206377616444));
#73184=CARTESIAN_POINT('Ctrl Pts',(157.320539922536,5.17619186681082,338.425265024517));
#73185=CARTESIAN_POINT('Ctrl Pts',(157.042301888262,5.68151286289929,332.50083727642));
#73186=CARTESIAN_POINT('Ctrl Pts',(156.764063853988,0.972993363697465,328.869854272171));
#73187=CARTESIAN_POINT('Ctrl Pts',(156.485825819714,-4.62842778401096,330.864415521548));
#73188=CARTESIAN_POINT('Ctrl Pts',(156.20758778544,-5.9824090698147,336.654141605673));
#73189=CARTESIAN_POINT('Ctrl Pts',(155.929349751166,-1.84642185246274,340.925886353362));
#73190=CARTESIAN_POINT('Ctrl Pts',(155.651111716892,3.98399944575246,339.759532660511));
#73191=CARTESIAN_POINT('Ctrl Pts',(155.372873682618,6.15836325633603,334.225426095694));
#73192=CARTESIAN_POINT('Ctrl Pts',(155.094635648344,2.68128800387271,329.402134570168));
#73193=CARTESIAN_POINT('Ctrl Pts',(154.81639761407,-3.25636567399855,329.715921525239));
#73194=CARTESIAN_POINT('Ctrl Pts',(154.538159579796,-6.2057006367199,334.878829303729));
#73195=CARTESIAN_POINT('Ctrl Pts',(154.259921545522,-3.46015572111465,340.152933641709));
#73196=CARTESIAN_POINT('Ctrl Pts',(153.981683511248,2.46072302794279,340.69826683387));
#73197=CARTESIAN_POINT('Ctrl Pts',(153.703445476974,6.12343257446949,336.014384658867));
#73198=CARTESIAN_POINT('Ctrl Pts',(153.4252074427,4.16675842912217,330.399616654718));
#73199=CARTESIAN_POINT('Ctrl Pts',(153.146969408426,-1.61368842537694,329.006552544985));
#73200=CARTESIAN_POINT('Ctrl Pts',(152.868731374152,-5.91327722990972,333.113586701582));
#73201=CARTESIAN_POINT('Ctrl Pts',(152.590493339879,-4.7863388003833,338.951754498722));
#73202=CARTESIAN_POINT('Ctrl Pts',(152.312255305605,0.732952100009919,341.163455520186));
#73203=CARTESIAN_POINT('Ctrl Pts',(152.034017271331,5.57962367657935,337.71904438323));
#73204=CARTESIAN_POINT('Ctrl Pts',(151.755779237057,5.30595696026238,331.779406348814));
#73205=CARTESIAN_POINT('Ctrl Pts',(151.477541202783,0.163091857308978,328.795259572205));
#73206=CARTESIAN_POINT('Ctrl Pts',(151.199303168509,-5.12944023586499,331.505111504367));
#73207=CARTESIAN_POINT('Ctrl Pts',(150.921065134235,-5.71476073499945,337.4221710245));
#73208=CARTESIAN_POINT('Ctrl Pts',(150.642827099961,-1.05572965735508,341.116439946636));
#73209=CARTESIAN_POINT('Ctrl Pts',(150.364589065687,4.57212894429984,339.197742208249));
#73210=CARTESIAN_POINT('Ctrl Pts',(150.086351031413,6.0042122982834,333.426838403926));
#73211=CARTESIAN_POINT('Ctrl Pts',(149.808112997139,1.92631864816058,329.099601776493));
#73212=CARTESIAN_POINT('Ctrl Pts',(149.529874962865,-3.91932919296249,330.187073509037));
#73213=CARTESIAN_POINT('Ctrl Pts',(149.251636928591,-6.16826648290805,335.69129684366));
#73214=CARTESIAN_POINT('Ctrl Pts',(148.973398894317,-2.75667666495296,340.561127268381));
#73215=CARTESIAN_POINT('Ctrl Pts',(148.695160860043,3.18467463994858,340.327593281013));
#73216=CARTESIAN_POINT('Ctrl Pts',(148.41692282577,6.20349703348994,335.205005574807));
#73217=CARTESIAN_POINT('Ctrl Pts',(148.138684791495,3.52946176286371,329.894287278479));
#73218=CARTESIAN_POINT('Ctrl Pts',(147.860446757222,-2.38350847277232,329.269006186494));
#73219=CARTESIAN_POINT('Ctrl Pts',(147.582208722948,-6.10916816347259,333.902973527834));
#73220=CARTESIAN_POINT('Ctrl Pts',(147.303970688674,-4.22853440172834,339.543665870596));
#73221=CARTESIAN_POINT('Ctrl Pts',(147.0257326544,1.53256296741654,341.014703108311));
#73222=CARTESIAN_POINT('Ctrl Pts',(146.747494620126,5.88724992195559,336.966136080401));
#73223=CARTESIAN_POINT('Ctrl Pts',(146.469256585852,4.8392945187824,331.113274991628));
#73224=CARTESIAN_POINT('Ctrl Pts',(146.191018551578,-0.649610036407337,
328.827204075071));
#73225=CARTESIAN_POINT('Ctrl Pts',(145.912780517304,-5.54237704941444,332.205816868504));
#73226=CARTESIAN_POINT('Ctrl Pts',(145.63454248303,-5.3489864495252,338.148610279633));
#73227=CARTESIAN_POINT('Ctrl Pts',(145.356304448756,-0.246909935817251,
341.201970510557));
#73228=CARTESIAN_POINT('Ctrl Pts',(145.078066414482,5.08175218160551,338.563873944876));
#73229=CARTESIAN_POINT('Ctrl Pts',(144.799828380208,5.74696532850814,332.655262862677));
#73230=CARTESIAN_POINT('Ctrl Pts',(144.521590345935,1.13827321850806,328.898382443135));
#73231=CARTESIAN_POINT('Ctrl Pts',(144.24335231166,-4.51499542323171,330.740866395801));
#73232=CARTESIAN_POINT('Ctrl Pts',(143.965114277387,-6.02491940629494,336.491894392332));
#73233=CARTESIAN_POINT('Ctrl Pts',(143.686876243112,-2.00586377786598,340.873832925344));
#73234=CARTESIAN_POINT('Ctrl Pts',(143.408638208839,3.85394343300977,339.8654416804));
#73235=CARTESIAN_POINT('Ctrl Pts',(143.130400174565,6.17704363952428,334.392106419154));
#73236=CARTESIAN_POINT('Ctrl Pts',(142.852162140291,2.83156207106203,329.476626124556));
#73237=CARTESIAN_POINT('Ctrl Pts',(142.573924106017,-3.11240221622613,329.629864510587));
#73238=CARTESIAN_POINT('Ctrl Pts',(142.295686071743,-6.200160928665,334.711196972183));
#73239=CARTESIAN_POINT('Ctrl Pts',(142.017448037469,-3.59812347109343,340.057559709681));
#73240=CARTESIAN_POINT('Ctrl Pts',(141.739210003195,2.30585878768524,340.762674551063));
#73241=CARTESIAN_POINT('Ctrl Pts',(141.460971968921,6.09378847142506,336.179468013873));
#73242=CARTESIAN_POINT('Ctrl Pts',(141.182733934647,4.28953841910852,330.51388108927));
#73243=CARTESIAN_POINT('Ctrl Pts',(140.904495900373,-1.45115772694064,328.965139274038));
#73244=CARTESIAN_POINT('Ctrl Pts',(140.626257866099,-5.8601478460293,332.954500072623));
#73245=CARTESIAN_POINT('Ctrl Pts',(140.348019831825,-4.89136678245731,338.820985963033));
#73246=CARTESIAN_POINT('Ctrl Pts',(140.069781797551,0.5661493809204,341.181009432828));
#73247=CARTESIAN_POINT('Ctrl Pts',(139.791543763277,5.50411861377862,337.868811777666));
#73248=CARTESIAN_POINT('Ctrl Pts',(139.513305729004,5.39103943542977,331.923947897733));
#73249=CARTESIAN_POINT('Ctrl Pts',(139.23506769473,0.330682938798655,328.801931629596));
#73250=CARTESIAN_POINT('Ctrl Pts',(138.956829660456,-5.03313640989581,331.367791221638));
#73251=CARTESIAN_POINT('Ctrl Pts',(138.678591626182,-5.77812076420052,337.266875198271));
#73252=CARTESIAN_POINT('Ctrl Pts',(138.400353591908,-1.22060897812122,341.085681264472));
#73253=CARTESIAN_POINT('Ctrl Pts',(138.122115557634,4.45703765102095,339.319747458776));
#73254=CARTESIAN_POINT('Ctrl Pts',(137.84387752336,6.04452661358915,333.589645169529));
#73255=CARTESIAN_POINT('Ctrl Pts',(137.565639489086,2.08504271993315,329.153804691402));
#73256=CARTESIAN_POINT('Ctrl Pts',(137.287401454812,-3.7878541026254,330.082931358274));
#73257=CARTESIAN_POINT('Ctrl Pts',(137.009163420538,-6.18469312383953,335.524379341844));
#73258=CARTESIAN_POINT('Ctrl Pts',(136.730925386264,-2.90593055122699,340.48461214323));
#73259=CARTESIAN_POINT('Ctrl Pts',(136.45268735199,3.03956159678193,340.411697333516));
#73260=CARTESIAN_POINT('Ctrl Pts',(136.174449317716,6.1956929312797,335.372547757357));
#73261=CARTESIAN_POINT('Ctrl Pts',(135.896211283442,3.66612831101986,329.991516603066));
#73262=CARTESIAN_POINT('Ctrl Pts',(135.617973249168,-2.22778814829773,329.206696737048));
#73263=CARTESIAN_POINT('Ctrl Pts',(135.339735214895,-6.07729630602166,333.738305766426));
#73264=CARTESIAN_POINT('Ctrl Pts',(135.06149718062,-4.34975934445596,339.427752971376));
#73265=CARTESIAN_POINT('Ctrl Pts',(134.783259146347,1.36948756517418,341.053916628024));
#73266=CARTESIAN_POINT('Ctrl Pts',(134.505021112073,5.83197594984737,337.124490350795));
#73267=CARTESIAN_POINT('Ctrl Pts',(134.226783077799,4.94254608516959,331.24545063607));
#73268=CARTESIAN_POINT('Ctrl Pts',(133.948545043525,-0.482585370007687,
328.811905455564));
#73269=CARTESIAN_POINT('Ctrl Pts',(133.670307009251,-5.46485535407729,332.057083302363));
#73270=CARTESIAN_POINT('Ctrl Pts',(133.392068974977,-5.43210824084298,338.002932365204));
#73271=CARTESIAN_POINT('Ctrl Pts',(133.113830940703,-0.414395572773265,
341.193034719706));
#73272=CARTESIAN_POINT('Ctrl Pts',(132.835592906429,4.98360179596184,338.699880520978));
#73273=CARTESIAN_POINT('Ctrl Pts',(132.557354872155,5.8082213543847,332.811400578295));
#73274=CARTESIAN_POINT('Ctrl Pts',(132.279116837881,1.30272190509538,328.931366021237));
#73275=CARTESIAN_POINT('Ctrl Pts',(132.000878803607,-4.39826620835616,330.620427293599));
#73276=CARTESIAN_POINT('Ctrl Pts',(131.722640769333,-6.06303034070208,336.328557796239));
#73277=CARTESIAN_POINT('Ctrl Pts',(131.444402735059,-2.16384101956683,340.817490418751));
#73278=CARTESIAN_POINT('Ctrl Pts',(131.166164700785,3.72107326698374,339.967797949994));
#73279=CARTESIAN_POINT('Ctrl Pts',(130.887926666511,6.19121353937478,334.559230627104));
#73280=CARTESIAN_POINT('Ctrl Pts',(130.609688632238,2.97976852884374,329.555150851977));
#73281=CARTESIAN_POINT('Ctrl Pts',(130.331450597963,-2.96616607929583,329.547728774148));
#73282=CARTESIAN_POINT('Ctrl Pts',(130.05321256369,-6.1900938570052,334.543775524893));
#73283=CARTESIAN_POINT('Ctrl Pts',(129.774974529416,-3.73346386777644,339.958492742581));
#73284=CARTESIAN_POINT('Ctrl Pts',(129.496736495142,2.14931080707439,340.822874357635));
#73285=CARTESIAN_POINT('Ctrl Pts',(129.218498460868,6.05969467804856,336.343690120174));
#73286=CARTESIAN_POINT('Ctrl Pts',(128.940260426594,4.40918618392441,330.631421292261));
#73287=CARTESIAN_POINT('Ctrl Pts',(128.66202239232,-1.28756739170578,328.928132664326));
#73288=CARTESIAN_POINT('Ctrl Pts',(128.383784358046,-5.80273937643113,332.796907069723));
#73289=CARTESIAN_POINT('Ctrl Pts',(128.105546323772,-4.99282308369843,338.687427339638));
#73290=CARTESIAN_POINT('Ctrl Pts',(127.827308289498,0.398933258996397,341.194049966306));
#73291=CARTESIAN_POINT('Ctrl Pts',(127.549070255224,5.42459443815543,338.016484362922));
#73292=CARTESIAN_POINT('Ctrl Pts',(127.27083222095,5.47218536830197,332.070735582922));
#73293=CARTESIAN_POINT('Ctrl Pts',(126.992594186676,0.498032555281528,328.813129522603));
#73294=CARTESIAN_POINT('Ctrl Pts',(126.714356152402,-4.93315738277237,331.233123181331));
#73295=CARTESIAN_POINT('Ctrl Pts',(126.436118118129,-5.83726160393966,337.109924097544));
#73296=CARTESIAN_POINT('Ctrl Pts',(126.157880083854,-1.38459700901158,341.050478811867));
#73297=CARTESIAN_POINT('Ctrl Pts',(125.879642049581,4.33869182446808,339.438598425463));
#73298=CARTESIAN_POINT('Ctrl Pts',(125.601404015306,6.08042720961975,333.753481777615));
#73299=CARTESIAN_POINT('Ctrl Pts',(125.323165981033,2.24224429146187,329.212276503873));
#73300=CARTESIAN_POINT('Ctrl Pts',(125.044927946759,-3.65361311749906,329.982379655866));
#73301=CARTESIAN_POINT('Ctrl Pts',(124.766689912485,-6.19660369577232,335.357078937718));
#73302=CARTESIAN_POINT('Ctrl Pts',(124.488451878211,-3.05306252415595,340.404092148901));
#73303=CARTESIAN_POINT('Ctrl Pts',(124.210213843937,2.89222906274935,340.491849759308));
#73304=CARTESIAN_POINT('Ctrl Pts',(123.931975809663,6.18336472800057,335.539817905167));
#73305=CARTESIAN_POINT('Ctrl Pts',(123.653737775389,3.80011784867946,330.092403127154));
#73306=CARTESIAN_POINT('Ctrl Pts',(123.375499741115,-2.07044109072718,329.14861756334));
#73307=CARTESIAN_POINT('Ctrl Pts',(123.097261706841,-6.04098680083397,333.574559295386));
#73308=CARTESIAN_POINT('Ctrl Pts',(122.819023672567,-4.46780808863448,339.308606922586));
#73309=CARTESIAN_POINT('Ctrl Pts',(122.540785638293,1.20541216176558,341.088709571862));
#73310=CARTESIAN_POINT('Ctrl Pts',(122.26254760402,5.77244346316771,337.281293316247));
#73311=CARTESIAN_POINT('Ctrl Pts',(121.984309569745,5.04218859954669,331.380367856147));
#73312=CARTESIAN_POINT('Ctrl Pts',(121.706071535472,-0.315208319296592,
328.801125388777));
#73313=CARTESIAN_POINT('Ctrl Pts',(121.427833501198,-5.38334321598855,331.910498656888));
#73314=CARTESIAN_POINT('Ctrl Pts',(121.149595466924,-5.51126350138344,337.855061706608));
#73315=CARTESIAN_POINT('Ctrl Pts',(120.87135743265,-0.581578617674682,341.179576768816));
#73316=CARTESIAN_POINT('Ctrl Pts',(120.593119398376,4.8818123793878,338.833185440684));
#73317=CARTESIAN_POINT('Ctrl Pts',(120.314881364102,5.86523621131872,332.969136411362));
#73318=CARTESIAN_POINT('Ctrl Pts',(120.036643329828,1.46621934286705,328.968780921835));
#73319=CARTESIAN_POINT('Ctrl Pts',(119.758405295554,-4.27832537517161,330.503186159693));
#73320=CARTESIAN_POINT('Ctrl Pts',(119.48016726128,-6.09671404439443,336.164251085937));
#73321=CARTESIAN_POINT('Ctrl Pts',(119.201929227006,-2.32023822242827,340.756899974934));
#73322=CARTESIAN_POINT('Ctrl Pts',(118.923691192732,3.58548596960027,340.06652672864));
#73323=CARTESIAN_POINT('Ctrl Pts',(118.645453158458,6.20086260901282,334.726676685283));
#73324=CARTESIAN_POINT('Ctrl Pts',(118.367215124184,3.12579915671638,329.637651413598));
#73325=CARTESIAN_POINT('Ctrl Pts',(118.08897708991,-2.81776404497875,329.469574291517));
#73326=CARTESIAN_POINT('Ctrl Pts',(117.810739055636,-6.17550677272601,334.376687213162));
#73327=CARTESIAN_POINT('Ctrl Pts',(117.532501021362,-3.86607808547316,339.855805079206));
#73328=CARTESIAN_POINT('Ctrl Pts',(117.254262987089,1.9911933975994,340.878822295629));
#73329=CARTESIAN_POINT('Ctrl Pts',(116.976024952814,6.02117608966137,336.506931062627));
#73330=CARTESIAN_POINT('Ctrl Pts',(116.697786918541,4.5256143566545,330.752151435719));
#73331=CARTESIAN_POINT('Ctrl Pts',(116.419548884267,-1.12303687349579,328.895559738109));
#73332=CARTESIAN_POINT('Ctrl Pts',(116.141310849993,-5.74109374083608,332.640922767447));
#73333=CARTESIAN_POINT('Ctrl Pts',(115.863072815719,-5.09063362061581,338.551176153174));
#73334=CARTESIAN_POINT('Ctrl Pts',(115.584834781445,0.231425835614517,341.202567598409));
#73335=CARTESIAN_POINT('Ctrl Pts',(115.306596747171,5.34110921834113,338.161954308331));
#73336=CARTESIAN_POINT('Ctrl Pts',(115.028358712897,5.54933550603892,332.219662219867));
#73337=CARTESIAN_POINT('Ctrl Pts',(114.750120678623,0.665018507902607,328.828845074513));
#73338=CARTESIAN_POINT('Ctrl Pts',(114.471882644349,-4.82957615927886,331.101205718181));
#73339=CARTESIAN_POINT('Ctrl Pts',(114.193644610075,-5.89214006951734,336.951432328165));
#73340=CARTESIAN_POINT('Ctrl Pts',(113.915406575801,-1.54757400580489,341.010858293686));
#73341=CARTESIAN_POINT('Ctrl Pts',(113.637168541527,4.21717788087984,339.554208323215));
#73342=CARTESIAN_POINT('Ctrl Pts',(113.358930507253,6.11188787172474,333.918228594534));
#73343=CARTESIAN_POINT('Ctrl Pts',(113.080692472979,2.39780857400497,329.27497451773));
#73344=CARTESIAN_POINT('Ctrl Pts',(112.802454438706,-3.51670426048264,329.885491824767));
#73345=CARTESIAN_POINT('Ctrl Pts',(112.524216404431,-6.20398950159512,335.189517794199));
#73346=CARTESIAN_POINT('Ctrl Pts',(112.245978370158,-3.1979651478287,340.319626081173));
#73347=CARTESIAN_POINT('Ctrl Pts',(111.967740335884,2.74278462021191,340.567992031006));
#73348=CARTESIAN_POINT('Ctrl Pts',(111.68950230161,6.16652142571869,335.706693877412));
#73349=CARTESIAN_POINT('Ctrl Pts',(111.411264267336,3.93133253655047,330.196873183302));
#73350=CARTESIAN_POINT('Ctrl Pts',(111.133026233062,-1.91158219503698,329.09481107484));
#73351=CARTESIAN_POINT('Ctrl Pts',(110.854788198788,-6.00026616114596,333.41185368255));
#73352=CARTESIAN_POINT('Ctrl Pts',(110.576550164514,-4.58259443495464,339.186314724784));
#73353=CARTESIAN_POINT('Ctrl Pts',(110.29831213024,1.04045656521155,341.119056533987));
#73354=CARTESIAN_POINT('Ctrl Pts',(110.020074095966,5.70869593259684,337.436430479077));
#73355=CARTESIAN_POINT('Ctrl Pts',(109.741836061692,5.13814930285185,331.517928135172));
#73356=CARTESIAN_POINT('Ctrl Pts',(109.463598027418,-0.147601103160891,
328.794871746324));
#73357=CARTESIAN_POINT('Ctrl Pts',(109.185359993144,-5.29790015539158,331.766169968332));
#73358=CARTESIAN_POINT('Ctrl Pts',(108.90712195887,-5.58639443189754,337.705106279148));
#73359=CARTESIAN_POINT('Ctrl Pts',(108.628883924596,-0.748336993297773,
341.161606484894));
#73360=CARTESIAN_POINT('Ctrl Pts',(108.350645890323,4.77645825861544,338.963691364615));
#73361=CARTESIAN_POINT('Ctrl Pts',(108.072407856048,5.9179682670056,333.128355183018));
#73362=CARTESIAN_POINT('Ctrl Pts',(107.794169821775,1.62864614583315,329.010599824533));
#73363=CARTESIAN_POINT('Ctrl Pts',(107.515931787501,-4.15526050459266,330.389228603673));
#73364=CARTESIAN_POINT('Ctrl Pts',(107.237693753227,-6.12594592149832,335.999094238348));
#73365=CARTESIAN_POINT('Ctrl Pts',(106.959455718953,-2.47494118505861,340.692105837097));
#73366=CARTESIAN_POINT('Ctrl Pts',(106.681217684679,3.44728054683719,340.161555924489));
#73367=CARTESIAN_POINT('Ctrl Pts',(106.402979650405,6.20598380267818,334.894322324416));
#73368=CARTESIAN_POINT('Ctrl Pts',(106.124741616131,3.26954732297222,329.724067567429));
#73369=CARTESIAN_POINT('Ctrl Pts',(105.846503581857,-2.66730447658596,329.395458131174));
#73370=CARTESIAN_POINT('Ctrl Pts',(105.568265547583,-6.15641032733074,334.210054045042));
#73371=CARTESIAN_POINT('Ctrl Pts',(105.290027513309,-3.99586928915159,339.749571702188));
#73372=CARTESIAN_POINT('Ctrl Pts',(105.011789479035,1.83162201674796,340.930477511803));
#73373=CARTESIAN_POINT('Ctrl Pts',(104.733551444761,5.97826083257455,336.669071642537));
#73374=CARTESIAN_POINT('Ctrl Pts',(104.455313410487,4.63873792133273,330.875983362375));
#73375=CARTESIAN_POINT('Ctrl Pts',(104.177075376213,-0.957686312656652,
328.867444280173));
#73376=CARTESIAN_POINT('Ctrl Pts',(103.898837341939,-5.67525595294783,332.486661065683));
#73377=CARTESIAN_POINT('Ctrl Pts',(103.620599307666,-5.18472697185933,338.412331894394));
#73378=CARTESIAN_POINT('Ctrl Pts',(103.342361273392,0.0637494248598003,
341.206556109554));
#73379=CARTESIAN_POINT('Ctrl Pts',(103.064123239118,5.25372391532508,338.305115391596));
#73380=CARTESIAN_POINT('Ctrl Pts',(102.785885204844,5.62243351353439,332.370619062192));
#73381=CARTESIAN_POINT('Ctrl Pts',(102.50764717057,0.831518863355839,328.849066809817));
#73382=CARTESIAN_POINT('Ctrl Pts',(102.229409136296,-4.72246837452607,330.972135158446));
#73383=CARTESIAN_POINT('Ctrl Pts',(101.951171102022,-5.94271608862435,336.791515620983));
#73384=CARTESIAN_POINT('Ctrl Pts',(101.672933067748,-1.70942096253776,340.96684864087));
#73385=CARTESIAN_POINT('Ctrl Pts',(101.394695033474,4.0925845498577,339.666492733573));
#73386=CARTESIAN_POINT('Ctrl Pts',(101.1164569992,6.13888562729768,334.083765321995));
#73387=CARTESIAN_POINT('Ctrl Pts',(100.838218964926,2.55162197436991,329.341852950821));
#73388=CARTESIAN_POINT('Ctrl Pts',(100.559980930652,-3.37722750255852,329.792338612565));
#73389=CARTESIAN_POINT('Ctrl Pts',(100.281742896378,-6.20684514818521,335.021818264602));
#73390=CARTESIAN_POINT('Ctrl Pts',(100.003504862104,-3.34053261420657,340.231275617251));
#73391=CARTESIAN_POINT('Ctrl Pts',(99.7252668278303,2.59133739364889,340.64006854945));
#73392=CARTESIAN_POINT('Ctrl Pts',(99.4470287935565,6.14517532342992,335.873053821095));
#73393=CARTESIAN_POINT('Ctrl Pts',(99.1687907592825,4.05967656153864,330.304850487373));
#73394=CARTESIAN_POINT('Ctrl Pts',(98.8905527250086,-1.75132746014872,329.045316561097));
#73395=CARTESIAN_POINT('Ctrl Pts',(98.6123146907346,-5.95516412120866,333.250307735717));
#73396=CARTESIAN_POINT('Ctrl Pts',(98.3340766564607,-4.69403456631375,339.060965675855));
#73397=CARTESIAN_POINT('Ctrl Pts',(98.0558386221866,0.874741226250659,341.144935355016));
#73398=CARTESIAN_POINT('Ctrl Pts',(97.7776005879129,5.64077990664417,337.589788557975));
#73399=CARTESIAN_POINT('Ctrl Pts',(97.4993625536387,5.23035812448528,331.658031026498));
#73400=CARTESIAN_POINT('Ctrl Pts',(97.221124519365,0.0201138914456118,328.793149094622));
#73401=CARTESIAN_POINT('Ctrl Pts',(96.9428864850909,-5.20858856289313,331.624202625643));
#73402=CARTESIAN_POINT('Ctrl Pts',(96.6646484508171,-5.65744617170602,337.553175580424));
#73403=CARTESIAN_POINT('Ctrl Pts',(96.3864104165431,-0.914548932512907,
341.139136989859));
#73404=CARTESIAN_POINT('Ctrl Pts',(96.1081723822692,4.66761636332718,339.091302997216));
#73405=CARTESIAN_POINT('Ctrl Pts',(95.8299343479952,5.96637901644651,333.288940631558));
#73406=CARTESIAN_POINT('Ctrl Pts',(95.5516963137214,1.78988370978281,329.056792193128));
#73407=CARTESIAN_POINT('Ctrl Pts',(95.2734582794472,-4.02916145870834,330.278637837457));
#73408=CARTESIAN_POINT('Ctrl Pts',(94.9952202451736,-6.15070462686848,335.833207851163));
#73409=CARTESIAN_POINT('Ctrl Pts',(94.7169822108993,-2.62783694320291,340.623155317982));
#73410=CARTESIAN_POINT('Ctrl Pts',(94.4387441766256,3.30655791643028,340.252816147127));
#73411=CARTESIAN_POINT('Ctrl Pts',(94.1605061423516,6.20657338087024,335.062045129492));
#73412=CARTESIAN_POINT('Ctrl Pts',(93.8822681080776,3.41090806255851,329.814336212306));
#73413=CARTESIAN_POINT('Ctrl Pts',(93.6040300738037,-2.51489723984268,329.325434412816));
#73414=CARTESIAN_POINT('Ctrl Pts',(93.3257920395297,-6.13281846506266,334.043997696233));
#73415=CARTESIAN_POINT('Ctrl Pts',(93.0475540052558,-4.1227427051468,339.639870183246));
#73416=CARTESIAN_POINT('Ctrl Pts',(92.7693159709819,1.67071318369969,340.977802287466));
#73417=CARTESIAN_POINT('Ctrl Pts',(92.4910779367078,5.93098024355116,336.829993464695));
#73418=CARTESIAN_POINT('Ctrl Pts',(92.2128399024341,4.74847427502061,331.002826650033));
#73419=CARTESIAN_POINT('Ctrl Pts',(91.9346018681601,-0.79163644833082,328.843806820454));
#73420=CARTESIAN_POINT('Ctrl Pts',(91.6563638338862,-5.60527408758383,332.334234606481));
#73421=CARTESIAN_POINT('Ctrl Pts',(91.3781257996122,-5.27503443037134,338.270995947509));
#73422=CARTESIAN_POINT('Ctrl Pts',(91.0998877653383,-0.103973535787613,
341.206012587328));
#73423=CARTESIAN_POINT('Ctrl Pts',(90.8216497310643,5.16250233794153,338.445863076353));
#73424=CARTESIAN_POINT('Ctrl Pts',(90.5434116967905,5.69142601455134,332.523495881063));
#73425=CARTESIAN_POINT('Ctrl Pts',(90.2651736625165,0.997412042917653,328.873779962582));
#73426=CARTESIAN_POINT('Ctrl Pts',(89.9869356282425,-4.61191223872394,330.846005749579));
#73427=CARTESIAN_POINT('Ctrl Pts',(89.7086975939687,-5.98895273060163,336.630290747333));
#73428=CARTESIAN_POINT('Ctrl Pts',(89.4304595596946,-1.87001969840361,340.918481989311));
#73429=CARTESIAN_POINT('Ctrl Pts',(89.1522215254208,3.9650028095739,339.77536966635));
#73430=CARTESIAN_POINT('Ctrl Pts',(88.8739834911467,6.16140076255098,334.249971084919));
#73431=CARTESIAN_POINT('Ctrl Pts',(88.5957454568728,2.70357217786121,329.41286296845));
#73432=CARTESIAN_POINT('Ctrl Pts',(88.317507422599,-3.23528468979185,329.702988039827));
#73433=CARTESIAN_POINT('Ctrl Pts',(88.0392693883248,-6.20516855034669,334.854102803286));
#73434=CARTESIAN_POINT('Ctrl Pts',(87.7610313540511,-3.48066082038602,340.139105270731));
#73435=CARTESIAN_POINT('Ctrl Pts',(87.482793319777,2.43799796997338,340.708026684295));
#73436=CARTESIAN_POINT('Ctrl Pts',(87.2045552855032,6.11934200807928,336.038776260018));
#73437=CARTESIAN_POINT('Ctrl Pts',(86.9263172512292,4.1850562067108,330.416256194235));
#73438=CARTESIAN_POINT('Ctrl Pts',(86.6480792169553,-1.58979390422782,329.000170163055));
#73439=CARTESIAN_POINT('Ctrl Pts',(86.3698411826813,-5.90571361457614,333.090039415897));
#73440=CARTESIAN_POINT('Ctrl Pts',(86.0916031484074,-4.80204710901799,338.932651305798));
#73441=CARTESIAN_POINT('Ctrl Pts',(85.8133651141335,0.70838715038682,341.166327138207));
#73442=CARTESIAN_POINT('Ctrl Pts',(85.5351270798595,5.56874497765884,337.741255570723));
#73443=CARTESIAN_POINT('Ctrl Pts',(85.2568890455857,5.31874773347449,331.800574226852));
#73444=CARTESIAN_POINT('Ctrl Pts',(84.9786510113115,0.187814198868455,328.795958691553));
#73445=CARTESIAN_POINT('Ctrl Pts',(84.7004129770378,-5.11547365390613,331.484700293515));
#73446=CARTESIAN_POINT('Ctrl Pts',(84.4221749427637,-5.7243668387584,337.399380550381));
#73447=CARTESIAN_POINT('Ctrl Pts',(84.1439369084899,-1.08009306719839,341.11218469096));
#73448=CARTESIAN_POINT('Ctrl Pts',(83.865698874216,4.55536616998208,339.215927156345));
#73449=CARTESIAN_POINT('Ctrl Pts',(83.5874608399418,6.01043311006456,333.450775497334));
#73450=CARTESIAN_POINT('Ctrl Pts',(83.3092228056682,1.94981429888808,329.107324297904));
#73451=CARTESIAN_POINT('Ctrl Pts',(83.0309847713939,-3.90012031516611,330.171494614536));
#73452=CARTESIAN_POINT('Ctrl Pts',(82.7527467371202,-6.17097208167385,335.666713054786));
#73453=CARTESIAN_POINT('Ctrl Pts',(82.4745087028461,-2.77881385222812,340.550098765327));
#73454=CARTESIAN_POINT('Ctrl Pts',(82.1962706685723,3.16342083418214,340.340240758251));
#73455=CARTESIAN_POINT('Ctrl Pts',(81.9180326342983,6.20263091307842,335.229722629152));
#73456=CARTESIAN_POINT('Ctrl Pts',(81.6397946000243,3.54977815372484,329.908391433981));
#73457=CARTESIAN_POINT('Ctrl Pts',(81.3615565657505,-2.36065362266235,329.259554267826));
#73458=CARTESIAN_POINT('Ctrl Pts',(81.0833185314764,-6.10474841272267,333.878639421248));
#73459=CARTESIAN_POINT('Ctrl Pts',(80.8050804972027,-4.24660569036626,339.526780626535));
#73460=CARTESIAN_POINT('Ctrl Pts',(80.5268424629285,1.50858439424203,341.020762066024));
#73461=CARTESIAN_POINT('Ctrl Pts',(80.2486044286548,5.87936884692356,336.989579023824));
#73462=CARTESIAN_POINT('Ctrl Pts',(79.9703663943807,4.85474328812528,331.132588677602));
#73463=CARTESIAN_POINT('Ctrl Pts',(79.6921283601069,-0.625008530292098,
328.824664619043));
#73464=CARTESIAN_POINT('Ctrl Pts',(79.4138903258329,-5.5311992455712,332.183754691791));
#73465=CARTESIAN_POINT('Ctrl Pts',(79.1356522915589,-5.36149005355665,338.127271516167));
#73466=CARTESIAN_POINT('Ctrl Pts',(78.8574142572851,-0.271620574856635,
341.20093742861));
#73467=CARTESIAN_POINT('Ctrl Pts',(78.579176223011,5.0675110962762,338.584094588503));
#73468=CARTESIAN_POINT('Ctrl Pts',(78.3009381887372,5.75626263069755,332.678181045677));
#73469=CARTESIAN_POINT('Ctrl Pts',(78.0227001544631,1.16257691122491,328.902966487241));
#73470=CARTESIAN_POINT('Ctrl Pts',(77.7444621201893,-4.49798848007174,330.722909591397));
#73471=CARTESIAN_POINT('Ctrl Pts',(77.4662240859153,-6.0308162334077,336.467875433777));
#73472=CARTESIAN_POINT('Ctrl Pts',(77.1879860516414,-2.0292529440471,340.865793656386));
#73473=CARTESIAN_POINT('Ctrl Pts',(76.9097480173673,3.83452582034105,339.880759619502));
#73474=CARTESIAN_POINT('Ctrl Pts',(76.6315099830936,6.17941683691064,334.416724519695));
#73475=CARTESIAN_POINT('Ctrl Pts',(76.3532719488195,2.85354823029058,329.487952719032));
#73476=CARTESIAN_POINT('Ctrl Pts',(76.0750339145457,-3.09097946896438,329.617505350429));
#73477=CARTESIAN_POINT('Ctrl Pts',(75.7967958802716,-6.19896093233291,334.686493876246));
#73478=CARTESIAN_POINT('Ctrl Pts',(75.5185578459978,-3.6182474446129,340.04318234449));
#73479=CARTESIAN_POINT('Ctrl Pts',(75.2403198117237,2.28287831778362,340.771816812444));
#73480=CARTESIAN_POINT('Ctrl Pts',(74.9620817774499,6.08904034317885,336.203740183496));
#73481=CARTESIAN_POINT('Ctrl Pts',(74.6838437431759,4.30737991972699,330.531008955329));
#73482=CARTESIAN_POINT('Ctrl Pts',(74.4056057089021,-1.42709947923493,328.959404846657));
#73483=CARTESIAN_POINT('Ctrl Pts',(74.1273676746279,-5.85195075005674,332.93116575117));
#73484=CARTESIAN_POINT('Ctrl Pts',(73.8491296403542,-4.90655319220296,338.801465309891));
#73485=CARTESIAN_POINT('Ctrl Pts',(73.5708916060801,0.541515809529054,341.183216263261));
#73486=CARTESIAN_POINT('Ctrl Pts',(73.2926535718063,5.49264374561652,337.890720915959));
#73487=CARTESIAN_POINT('Ctrl Pts',(73.0144155375323,5.40325358764049,331.945453651052));
#73488=CARTESIAN_POINT('Ctrl Pts',(72.7361775032584,0.355377364179016,328.803298485545));
#73489=CARTESIAN_POINT('Ctrl Pts',(72.4579394689843,-5.01862342102826,331.347764836688));
#73490=CARTESIAN_POINT('Ctrl Pts',(72.1797014347105,-5.78710756751815,337.243833490301));
#73491=CARTESIAN_POINT('Ctrl Pts',(71.9014634004365,-1.24484851686434,341.080769268791));
#73492=CARTESIAN_POINT('Ctrl Pts',(71.6232253661627,4.4397896437819,339.33747284132));
#73493=CARTESIAN_POINT('Ctrl Pts',(71.3449873318886,6.05009837951721,333.613741608363));
#73494=CARTESIAN_POINT('Ctrl Pts',(71.0667492976148,2.10832113167528,329.16215924027));
#73495=CARTESIAN_POINT('Ctrl Pts',(70.7885112633407,-3.76823129993616,330.067877170995));
#73496=CARTESIAN_POINT('Ctrl Pts',(70.510273229067,-6.18673348659899,335.499731423882));
#73497=CARTESIAN_POINT('Ctrl Pts',(70.2320351947928,-2.92776166864652,340.472989525097));
#73498=CARTESIAN_POINT('Ctrl Pts',(69.953797160519,3.01797381893149,340.423765920324));
#73499=CARTESIAN_POINT('Ctrl Pts',(69.675559126245,6.19415927809661,335.397232385123));
#73500=CARTESIAN_POINT('Ctrl Pts',(69.3973210919711,3.68605619339361,330.006164553235));
#73501=CARTESIAN_POINT('Ctrl Pts',(69.1190830576973,-2.20468625388628,329.197865801953));
#73502=CARTESIAN_POINT('Ctrl Pts',(68.8408450234231,-6.07222066709064,333.714099964859));
#73503=CARTESIAN_POINT('Ctrl Pts',(68.5626069891494,-4.36736779993612,339.41038561016));
#73504=CARTESIAN_POINT('Ctrl Pts',(68.2843689548753,1.34535403497671,341.059325478203));
#73505=CARTESIAN_POINT('Ctrl Pts',(68.0061309206015,5.82346432938442,337.147711790396));
#73506=CARTESIAN_POINT('Ctrl Pts',(67.7278928863274,4.95746736290866,331.265174692718));
#73507=CARTESIAN_POINT('Ctrl Pts',(67.4496548520537,-0.457924230410055,
328.810031653601));
#73508=CARTESIAN_POINT('Ctrl Pts',(67.1714168177795,-5.45308551643202,332.035331202191));
#73509=CARTESIAN_POINT('Ctrl Pts',(66.8931787835057,-5.44403071143462,337.981263548091));
#73510=CARTESIAN_POINT('Ctrl Pts',(66.6149407492317,-0.439069276315245,
341.191334339285));
#73511=CARTESIAN_POINT('Ctrl Pts',(66.3367027149577,4.96881955302673,338.719708991262));
#73512=CARTESIAN_POINT('Ctrl Pts',(66.0584646806839,5.81689601821245,332.834561604773));
#73513=CARTESIAN_POINT('Ctrl Pts',(65.7802266464099,1.32689286472911,328.936605071765));
#73514=CARTESIAN_POINT('Ctrl Pts',(65.5019886121359,-4.38078028580957,330.602936568836));
#73515=CARTESIAN_POINT('Ctrl Pts',(65.2237505778621,-6.06827602827182,336.304388276137));
#73516=CARTESIAN_POINT('Ctrl Pts',(64.945512543588,-2.18700442719639,340.808822115166));
#73517=CARTESIAN_POINT('Ctrl Pts',(64.6672745093142,3.70124885658474,339.982585637181));
#73518=CARTESIAN_POINT('Ctrl Pts',(64.3890364750402,6.19292069502163,334.583903862799));
#73519=CARTESIAN_POINT('Ctrl Pts',(64.1107984407663,3.00144061899679,329.567067371956));
#73520=CARTESIAN_POINT('Ctrl Pts',(63.8325604064923,-2.94441721189048,329.535952963916));
#73521=CARTESIAN_POINT('Ctrl Pts',(63.5543223722184,-6.18822682695267,334.519113871686));
#73522=CARTESIAN_POINT('Ctrl Pts',(63.2760843379444,-3.75319202099864,339.943576881544));
#73523=CARTESIAN_POINT('Ctrl Pts',(62.9978463036705,2.12609170560242,340.831392354283));
#73524=CARTESIAN_POINT('Ctrl Pts',(62.7196082693966,6.05429245503427,336.367825134707));
#73525=CARTESIAN_POINT('Ctrl Pts',(62.4413702351226,4.42655837969133,330.649024978076));
#73526=CARTESIAN_POINT('Ctrl Pts',(62.1631322008487,-1.26336298479978,328.92305037878));
#73527=CARTESIAN_POINT('Ctrl Pts',(61.8848941665749,-5.7939147853471,332.773802751247));
#73528=CARTESIAN_POINT('Ctrl Pts',(61.6066561323007,-5.00747650542366,338.667503480278));
#73529=CARTESIAN_POINT('Ctrl Pts',(61.328418098027,0.37424905329486,341.195590397721));
#73530=CARTESIAN_POINT('Ctrl Pts',(61.0501800637529,5.41253177971177,338.038075453939));
#73531=CARTESIAN_POINT('Ctrl Pts',(60.771942029479,5.4838139807253,332.092563507999));
#73532=CARTESIAN_POINT('Ctrl Pts',(60.493703995205,0.522681032588899,328.815163117075));
#73533=CARTESIAN_POINT('Ctrl Pts',(60.2154659609312,-4.91810858439494,331.21349624557));
#73534=CARTESIAN_POINT('Ctrl Pts',(59.9372279266572,-5.84562254464326,337.0866479808));
#73535=CARTESIAN_POINT('Ctrl Pts',(59.6589898923833,-1.40869497691978,341.044913662926));
#73536=CARTESIAN_POINT('Ctrl Pts',(59.3807518581093,4.32097117881919,339.455851299363));
#73537=CARTESIAN_POINT('Ctrl Pts',(59.1025138238355,6.08534586118586,333.777719966632));
#73538=CARTESIAN_POINT('Ctrl Pts',(58.8242757895614,2.26528846629994,329.2212569797));
#73539=CARTESIAN_POINT('Ctrl Pts',(58.5460377552876,-3.63359071850647,329.967861168389));
#73540=CARTESIAN_POINT('Ctrl Pts',(58.2677997210135,-6.1979773326506,335.332384888601));
#73541=CARTESIAN_POINT('Ctrl Pts',(57.9895616867397,-3.07457163061672,340.391883902536));
#73542=CARTESIAN_POINT('Ctrl Pts',(57.7113236524656,2.87032307623123,340.50333064319));
#73543=CARTESIAN_POINT('Ctrl Pts',(57.4330856181918,6.18116466192095,335.564452081615));
#73544=CARTESIAN_POINT('Ctrl Pts',(57.1548475839177,3.81964267120667,330.107584176042));
#73545=CARTESIAN_POINT('Ctrl Pts',(56.876609549644,-2.04710902104055,329.140414060174));
#73546=CARTESIAN_POINT('Ctrl Pts',(56.5983715153699,-6.03525897995848,333.55049947394));
#73547=CARTESIAN_POINT('Ctrl Pts',(56.3201334810961,-4.48494085324504,339.290770125876));
#73548=CARTESIAN_POINT('Ctrl Pts',(56.041895446822,1.1811412968729,341.09346436496));
#73549=CARTESIAN_POINT('Ctrl Pts',(55.7636574125481,5.76330751246754,337.304276295707));
#73550=CARTESIAN_POINT('Ctrl Pts',(55.4854193782742,5.05657149015016,331.400487880946));
#73551=CARTESIAN_POINT('Ctrl Pts',(55.2071813440003,-0.290505553805166,
328.799918609128));
#73552=CARTESIAN_POINT('Ctrl Pts',(54.9289433097263,-5.37098993888844,331.889072516663));
#73553=CARTESIAN_POINT('Ctrl Pts',(54.6507052754524,-5.52259613273534,337.833078658442));
#73554=CARTESIAN_POINT('Ctrl Pts',(54.3724672411784,-0.606197368956423,
341.177210331541));
#73555=CARTESIAN_POINT('Ctrl Pts',(54.0942292069045,4.86649977285522,338.85260725886));
#73556=CARTESIAN_POINT('Ctrl Pts',(53.8159911726306,5.87328190253675,332.992523369114));
#73557=CARTESIAN_POINT('Ctrl Pts',(53.5377531383566,1.49023991975911,328.974671153226));
#73558=CARTESIAN_POINT('Ctrl Pts',(53.2595151040827,-4.2603732414763,330.486174286314));
#73559=CARTESIAN_POINT('Ctrl Pts',(52.9812770698088,-6.10130476201488,336.139948652894));
#73560=CARTESIAN_POINT('Ctrl Pts',(52.7030390355348,-2.34315895756308,340.747608966329));
#73561=CARTESIAN_POINT('Ctrl Pts',(52.4248010012609,3.56526923727485,340.080773365931));
#73562=CARTESIAN_POINT('Ctrl Pts',(52.146562966987,6.20190247635333,334.751387039712));
#73563=CARTESIAN_POINT('Ctrl Pts',(51.868324932713,3.14714135281286,329.650149157628));
#73564=CARTESIAN_POINT('Ctrl Pts',(51.5900868984391,-2.79570493847374,329.458390429919));
#73565=CARTESIAN_POINT('Ctrl Pts',(51.3118488641651,-6.17297407226025,334.35208501065));
#73566=CARTESIAN_POINT('Ctrl Pts',(51.0336108298912,-3.88539601288147,339.840361613899));
#73567=CARTESIAN_POINT('Ctrl Pts',(50.7553727956172,1.96775261916748,340.886709807693));
#73568=CARTESIAN_POINT('Ctrl Pts',(50.4771347613433,6.01512371658749,336.53091129866));
#73569=CARTESIAN_POINT('Ctrl Pts',(50.1988967270694,4.54250456237568,330.770218087062));
#73570=CARTESIAN_POINT('Ctrl Pts',(49.9206586927955,-1.09870398147085,328.891133305488));
#73571=CARTESIAN_POINT('Ctrl Pts',(49.6424206585215,-5.73164809836577,332.618065322743));
#73572=CARTESIAN_POINT('Ctrl Pts',(49.3641826242476,-5.10474335437767,338.530863636018));
#73573=CARTESIAN_POINT('Ctrl Pts',(49.0859445899735,0.206709020034407,341.203440505983));
#73574=CARTESIAN_POINT('Ctrl Pts',(48.8077065556997,5.32846757778105,338.183211586237));
#73575=CARTESIAN_POINT('Ctrl Pts',(48.5294685214257,5.56037008745055,332.24179637793));
#73576=CARTESIAN_POINT('Ctrl Pts',(48.2512304871518,0.689603038794641,328.831543922576));
#73577=CARTESIAN_POINT('Ctrl Pts',(47.9729924528778,-4.81400254003894,331.081992563213));
#73578=CARTESIAN_POINT('Ctrl Pts',(47.694754418604,-5.8998690424398,336.927938798894));
#73579=CARTESIAN_POINT('Ctrl Pts',(47.4165163843299,-1.57151280651798,341.00464405516));
#73580=CARTESIAN_POINT('Ctrl Pts',(47.1382783500561,4.19899753645439,339.570976090407));
#73581=CARTESIAN_POINT('Ctrl Pts',(46.8600403157821,6.11614981732458,333.942590834985));
#73582=CARTESIAN_POINT('Ctrl Pts',(46.5818022815083,2.42060168505957,329.284574362962));
#73583=CARTESIAN_POINT('Ctrl Pts',(46.3035642472342,-3.49629688556238,329.871519638507));
#73584=CARTESIAN_POINT('Ctrl Pts',(46.0253262129604,-6.20469540956123,335.164795645547));
#73585=CARTESIAN_POINT('Ctrl Pts',(45.7470881786863,-3.21913653735961,340.306841121049));
#73586=CARTESIAN_POINT('Ctrl Pts',(45.4688501444124,2.72057642079944,340.578876828611));
#73587=CARTESIAN_POINT('Ctrl Pts',(45.1906121101385,6.163656553233,335.731259614644));
#73588=CARTESIAN_POINT('Ctrl Pts',(44.9123740758645,3.95044004218623,330.212576245691));
#73589=CARTESIAN_POINT('Ctrl Pts',(44.6341360415906,-1.8880369871754,329.087240993811));
#73590=CARTESIAN_POINT('Ctrl Pts',(44.3558980073167,-5.99389034078641,333.387957409729));
#73591=CARTESIAN_POINT('Ctrl Pts',(44.0776599730428,-4.59923899833415,339.168021517031));
#73592=CARTESIAN_POINT('Ctrl Pts',(43.7994219387688,1.01606608823303,341.123153798048));
#73593=CARTESIAN_POINT('Ctrl Pts',(43.5211839044949,5.69894232273963,337.459158216201));
#73594=CARTESIAN_POINT('Ctrl Pts',(43.2429458702208,5.15198330391888,331.53842943646));
#73595=CARTESIAN_POINT('Ctrl Pts',(42.9647078359471,-0.122874749759113,
328.794332870184));
#73596=CARTESIAN_POINT('Ctrl Pts',(42.686469801673,-5.28497245921135,331.745085433442));
#73597=CARTESIAN_POINT('Ctrl Pts',(42.4082317673992,-5.59712894891147,337.68282505197));
#73598=CARTESIAN_POINT('Ctrl Pts',(42.1299937331252,-0.772882815683387,
341.158575718739));
#73599=CARTESIAN_POINT('Ctrl Pts',(41.8517556988512,4.76062646976567,338.98269234885));
#73600=CARTESIAN_POINT('Ctrl Pts',(41.5735176645774,5.92537911064229,333.151950994864));
#73601=CARTESIAN_POINT('Ctrl Pts',(41.2952796303033,1.65249880013479,329.017136935732));
#73602=CARTESIAN_POINT('Ctrl Pts',(41.0170415960296,-4.13685526841409,330.372708003766));
#73603=CARTESIAN_POINT('Ctrl Pts',(40.7388035617553,-6.12987831702303,335.974676638024));
#73604=CARTESIAN_POINT('Ctrl Pts',(40.4605655274817,-2.49760251095559,340.682198907772));
#73605=CARTESIAN_POINT('Ctrl Pts',(40.1823274932075,3.42668625486317,340.175251108975));
#73606=CARTESIAN_POINT('Ctrl Pts',(39.9040894589337,6.20635562240021,334.919051754053));
#73607=CARTESIAN_POINT('Ctrl Pts',(39.6258514246597,3.2905440409194,329.737137409643));
#73608=CARTESIAN_POINT('Ctrl Pts',(39.3476133903858,-2.64495123856271,329.384874384678));
#73609=CARTESIAN_POINT('Ctrl Pts',(39.0693753561119,-6.15321380583211,334.185529257777));
#73610=CARTESIAN_POINT('Ctrl Pts',(38.7911373218379,-4.01476288477629,339.733611909445));
#73611=CARTESIAN_POINT('Ctrl Pts',(38.512899287564,1.80797667783569,340.937728779813));
#73612=CARTESIAN_POINT('Ctrl Pts',(38.23466125329,5.97156272888989,336.69287958968));
#73613=CARTESIAN_POINT('Ctrl Pts',(37.9564232190161,4.65513380376322,330.894499786959));
#73614=CARTESIAN_POINT('Ctrl Pts',(37.6781851847422,-0.93324270341463,328.863676932662));
#73615=CARTESIAN_POINT('Ctrl Pts',(37.3999471504682,-5.6651961563086,332.464067185281));
#73616=CARTESIAN_POINT('Ctrl Pts',(37.1217091161943,-5.19828271471637,338.391645551662));
#73617=CARTESIAN_POINT('Ctrl Pts',(36.8434710819203,0.0390180476439763,
341.206760855887));
#73618=CARTESIAN_POINT('Ctrl Pts',(36.5652330476464,5.24051252358688,338.326023334307));
#73619=CARTESIAN_POINT('Ctrl Pts',(36.2869950133724,5.63286600647216,332.393043290855));
#73620=CARTESIAN_POINT('Ctrl Pts',(36.0087569790986,0.856021496183908,328.85242894077));
#73621=CARTESIAN_POINT('Ctrl Pts',(35.7305189448245,-4.70638130629574,330.953349813738));
#73622=CARTESIAN_POINT('Ctrl Pts',(35.4522809105507,-5.94980745006201,336.767821834182));
#73623=CARTESIAN_POINT('Ctrl Pts',(35.1740428762767,-1.73318311592037,340.959989850402));
#73624=CARTESIAN_POINT('Ctrl Pts',(34.8958048420028,4.07395778196053,339.682763150217));
#73625=CARTESIAN_POINT('Ctrl Pts',(34.6175668077288,6.14248775485454,334.108233824547));
#73626=CARTESIAN_POINT('Ctrl Pts',(34.3393287734549,2.5741473780892,329.352065155644));
#73627=CARTESIAN_POINT('Ctrl Pts',(34.0610907391809,-3.35645005319558,329.778922930024));
#73628=CARTESIAN_POINT('Ctrl Pts',(33.7828527049071,-6.20688281178436,334.997086068551));
#73629=CARTESIAN_POINT('Ctrl Pts',(33.504614670633,-3.36135082743875,340.217923278958));
#73630=CARTESIAN_POINT('Ctrl Pts',(33.2263766363592,2.56884319779051,340.650349312687));
#73631=CARTESIAN_POINT('Ctrl Pts',(32.9481386020852,6.14164773647087,335.897533181182));
#73632=CARTESIAN_POINT('Ctrl Pts',(32.6699005678113,4.07835279796391,330.321064096874));
#73633=CARTESIAN_POINT('Ctrl Pts',(32.3916625335373,-1.7275863068459,329.038385429884));
#73634=CARTESIAN_POINT('Ctrl Pts',(32.1134244992634,-5.94814495699532,333.226592460602));
#73635=CARTESIAN_POINT('Ctrl Pts',(31.8351864649894,-4.71017877458579,339.042229414774));
#73636=CARTESIAN_POINT('Ctrl Pts',(31.5569484307155,0.85024894713638,341.148372098216));
#73637=CARTESIAN_POINT('Ctrl Pts',(31.2787103964415,5.63041575972536,337.612244456948));
#73638=CARTESIAN_POINT('Ctrl Pts',(31.0004723621677,5.24363313441479,331.678898634205));
#73639=CARTESIAN_POINT('Ctrl Pts',(30.7222343278936,0.0448457775499455,
328.793278515476));
#73640=CARTESIAN_POINT('Ctrl Pts',(30.4439962936198,-5.1950958874499,331.603475092036));
#73641=CARTESIAN_POINT('Ctrl Pts',(30.1657582593458,-5.66757473602656,337.530612444009));
#73642=CARTESIAN_POINT('Ctrl Pts',(29.8875202250719,-0.939003902617646,
341.135444107894));
#73643=CARTESIAN_POINT('Ctrl Pts',(29.6092821907979,4.65127695254862,339.10986927297));
#73644=CARTESIAN_POINT('Ctrl Pts',(29.331044156524,5.97314960109628,333.312728067814));
#73645=CARTESIAN_POINT('Ctrl Pts',(29.05280612225,1.81355102426149,329.06397141073));
#73646=CARTESIAN_POINT('Ctrl Pts',(28.7745680879761,-4.01031655956884,330.262620574382));
#73647=CARTESIAN_POINT('Ctrl Pts',(28.4963300537022,-6.15397582885823,335.808692913317));
#73648=CARTESIAN_POINT('Ctrl Pts',(28.2180920194283,-2.6502223125389,340.612639701989));
#73649=CARTESIAN_POINT('Ctrl Pts',(27.9398539851543,3.28560110277981,340.265949878572));
#73650=CARTESIAN_POINT('Ctrl Pts',(27.6616159508804,6.20627688147068,335.086775576883));
#73651=CARTESIAN_POINT('Ctrl Pts',(27.3833779166065,3.43154397053261,329.827968609094));
#73652=CARTESIAN_POINT('Ctrl Pts',(27.1051398823325,-2.49226619265724,329.315458509681));
#73653=CARTESIAN_POINT('Ctrl Pts',(26.8269018480586,-6.12896045663425,334.01956823224));
#73654=CARTESIAN_POINT('Ctrl Pts',(26.5486638137846,-4.14119817286605,339.623405716922));
#73655=CARTESIAN_POINT('Ctrl Pts',(26.2704257795108,1.64688055015648,340.984412016543));
#73656=CARTESIAN_POINT('Ctrl Pts',(25.9921877452367,5.92364130021749,336.853611738357));
#73657=CARTESIAN_POINT('Ctrl Pts',(25.7139497109629,4.76436386187118,331.021779327147));
#73658=CARTESIAN_POINT('Ctrl Pts',(25.4357116766889,-0.767099970618971,
328.840701308971));
#73659=CARTESIAN_POINT('Ctrl Pts',(25.157473642415,-5.59460748244911,332.311920788455));
#73660=CARTESIAN_POINT('Ctrl Pts',(24.879235608141,-5.28802628390677,338.249950884387));
#73661=CARTESIAN_POINT('Ctrl Pts',(24.6009975738671,-0.128701415763207,
341.205549022917));
#73662=CARTESIAN_POINT('Ctrl Pts',(24.3227595395931,5.14873084199648,338.466406416866));
#73663=CARTESIAN_POINT('Ctrl Pts',(24.0445215053192,5.70124880119865,332.546193806135));
#73664=CARTESIAN_POINT('Ctrl Pts',(23.7662834710453,1.02181488583519,328.877802921394));
#73665=CARTESIAN_POINT('Ctrl Pts',(23.4880454367713,-4.59532346829624,330.827661932208));
#73666=CARTESIAN_POINT('Ctrl Pts',(23.2098074024974,-5.9954013024354,336.606414004227));
#73667=CARTESIAN_POINT('Ctrl Pts',(22.9315693682235,-1.89358785330778,340.910983655199));
#73668=CARTESIAN_POINT('Ctrl Pts',(22.6533313339495,3.9459432194895,339.79113085177));
#73669=CARTESIAN_POINT('Ctrl Pts',(22.3750932996756,6.16434044178771,334.274527982648));
#73670=CARTESIAN_POINT('Ctrl Pts',(22.0968552654016,2.72581342617312,329.4236800759));
#73671=CARTESIAN_POINT('Ctrl Pts',(21.8186172311277,-3.21415233770034,329.690138657152));
#73672=CARTESIAN_POINT('Ctrl Pts',(21.5403791968537,-6.20453794207692,334.82937861931));
#73673=CARTESIAN_POINT('Ctrl Pts',(21.2621411625798,-3.50111065583944,340.125195304161));
#73674=CARTESIAN_POINT('Ctrl Pts',(20.9839031283059,2.41523420295332,340.717695906141));
#73675=CARTESIAN_POINT('Ctrl Pts',(20.705665094032,6.11515428249423,336.063151368109));
#73676=CARTESIAN_POINT('Ctrl Pts',(20.427427059758,4.20328753651943,330.432968511652));
#73677=CARTESIAN_POINT('Ctrl Pts',(20.1491890254841,-1.56587414129691,328.993883042778));
#73678=CARTESIAN_POINT('Ctrl Pts',(19.8709509912101,-5.89805623190951,333.066522455404));
#73679=CARTESIAN_POINT('Ctrl Pts',(19.5927129569362,-4.81767917366603,338.913485672627));
#73680=CARTESIAN_POINT('Ctrl Pts',(19.3144749226622,0.683810953422714,341.16910085103));
#73681=CARTESIAN_POINT('Ctrl Pts',(19.0362368883883,5.55777786158857,337.763423234226));
#73682=CARTESIAN_POINT('Ctrl Pts',(18.7579988541143,5.33145405884136,331.82179290343));
#73683=CARTESIAN_POINT('Ctrl Pts',(18.4797608198405,0.212533558428351,328.796756314898));
#73684=CARTESIAN_POINT('Ctrl Pts',(18.2015227855665,-5.10142585156417,331.464344896456));
#73685=CARTESIAN_POINT('Ctrl Pts',(17.9232847512926,-5.73388205449841,337.376551980354));
#73686=CARTESIAN_POINT('Ctrl Pts',(17.6450467170186,-1.10443932797984,341.10783238973));
#73687=CARTESIAN_POINT('Ctrl Pts',(17.3668086827447,4.53853106832805,339.23404516651));
#73688=CARTESIAN_POINT('Ctrl Pts',(17.0885706484707,6.01655849184008,333.474737188387));
#73689=CARTESIAN_POINT('Ctrl Pts',(16.8103326141968,1.97327899164818,329.115140379641));
#73690=CARTESIAN_POINT('Ctrl Pts',(16.5320945799228,-3.88084951362897,330.155992384111));
#73691=CARTESIAN_POINT('Ctrl Pts',(16.2538565456489,-6.17357970149395,335.642118680249));
#73692=CARTESIAN_POINT('Ctrl Pts',(15.975618511375,-2.80090691918455,340.538982141178));
#73693=CARTESIAN_POINT('Ctrl Pts',(15.697380477101,3.14211680154138,340.352803446391));
#73694=CARTESIAN_POINT('Ctrl Pts',(15.4191424428271,6.2016663110622,335.254436036101));
#73695=CARTESIAN_POINT('Ctrl Pts',(15.1409044085532,3.57003818336322,329.92257643095));
#73696=CARTESIAN_POINT('Ctrl Pts',(14.8626663742792,-2.33776129152583,329.250193492469));
#73697=CARTESIAN_POINT('Ctrl Pts',(14.5844283400053,-6.10023173449145,333.854323118942));
#73698=CARTESIAN_POINT('Ctrl Pts',(14.3061903057313,-4.26460955396873,339.509823509002));
#73699=CARTESIAN_POINT('Ctrl Pts',(14.0279522714575,1.48458186866264,341.026725429732));
#73700=CARTESIAN_POINT('Ctrl Pts',(13.7497142371834,5.87139442288012,337.012990377927));
#73701=CARTESIAN_POINT('Ctrl Pts',(13.4714762029096,4.87011497673675,331.151963767972));
#73702=CARTESIAN_POINT('Ctrl Pts',(13.1932381686356,-0.600397100545508,
328.822223211257));
#73703=CARTESIAN_POINT('Ctrl Pts',(12.9150001343617,-5.51993362094364,332.161737229679));
#73704=CARTESIAN_POINT('Ctrl Pts',(12.6367621000877,-5.37390853065834,338.105883099841));
#73705=CARTESIAN_POINT('Ctrl Pts',(12.3585240658138,-0.296326902116208,
341.199805891837));
#73706=CARTESIAN_POINT('Ctrl Pts',(12.0802860315399,5.05318955368163,338.604258326258));
#73707=CARTESIAN_POINT('Ctrl Pts',(11.8020479972659,5.76546853542933,332.701136092723));
#73708=CARTESIAN_POINT('Ctrl Pts',(11.523809962992,1.18686215094859,328.907647337068));
#73709=CARTESIAN_POINT('Ctrl Pts',(11.245571928718,-4.48091013133853,330.705020694665));
#73710=CARTESIAN_POINT('Ctrl Pts',(10.9673338944441,-6.03661728657534,336.443833171777));
#73711=CARTESIAN_POINT('Ctrl Pts',(10.6890958601702,-2.0526099293305,340.857661249031));
#73712=CARTESIAN_POINT('Ctrl Pts',(10.4108578258962,3.81504739780807,339.896000074094));
#73713=CARTESIAN_POINT('Ctrl Pts',(10.1326197916223,6.18169178455076,334.441351863707));
#73714=CARTESIAN_POINT('Ctrl Pts',(9.85438175734834,2.87548934076866,329.499366863342));
#73715=CARTESIAN_POINT('Ctrl Pts',(9.5761437230744,-3.06950813245751,329.605231588139));
#73716=CARTESIAN_POINT('Ctrl Pts',(9.29790568880045,-6.19766159226215,334.661795875251));
#73717=CARTESIAN_POINT('Ctrl Pts',(9.01966765452654,-3.63831570770535,340.028724685263));
#73718=CARTESIAN_POINT('Ctrl Pts',(8.74142962025257,2.25986488325026,340.780867850567));
#73719=CARTESIAN_POINT('Ctrl Pts',(8.46319158597866,6.08418934066576,336.227992451325));
#73720=CARTESIAN_POINT('Ctrl Pts',(8.18495355170471,4.32516473003851,330.548209268121));
#73721=CARTESIAN_POINT('Ctrl Pts',(7.90671551743075,-1.40304066423951,328.953763513228));
#73722=CARTESIAN_POINT('Ctrl Pts',(7.62847748315686,-5.84361902743119,332.907869592604));
#73723=CARTESIAN_POINT('Ctrl Pts',(7.35023944888287,-4.92174046128214,338.781874263245));
#73724=CARTESIAN_POINT('Ctrl Pts',(7.07200141460898,0.517022360924158,341.185343870472));
#73725=CARTESIAN_POINT('Ctrl Pts',(6.79376338033501,5.48080084698006,337.91254837672));
#73726=CARTESIAN_POINT('Ctrl Pts',(6.51552534606109,5.41591225410207,331.967075452871));
#73727=CARTESIAN_POINT('Ctrl Pts',(6.23728731178713,0.37906437176057,328.804636265691));
#73728=CARTESIAN_POINT('Ctrl Pts',(5.95904927751322,-5.00213548323109,331.328036418174));
#73729=CARTESIAN_POINT('Ctrl Pts',(5.68081124323926,-5.79961147366261,337.220308739124));
#73730=CARTESIAN_POINT('Ctrl Pts',(5.40257320896532,-1.26200573051318,341.0765584996));
#73731=CARTESIAN_POINT('Ctrl Pts',(5.17070818040372,3.46225453493836,339.641128094155));
#73732=CARTESIAN_POINT('Ctrl Pts',(4.98521615755441,5.25418438838292,336.493556731435));
#73733=CARTESIAN_POINT('Ctrl Pts',(4.89247014612976,5.31273941270785,334.700718340289));
#73734=CARTESIAN_POINT('Ctrl Pts',(4.84609714041744,5.12095026465303,333.848094201961));
#73735=CARTESIAN_POINT('Ctrl Pts',(185.228765085591,2.85368302903013,338.999449094237));
#73736=CARTESIAN_POINT('Ctrl Pts',(185.182382275899,3.51972456975641,338.524219201027));
#73737=CARTESIAN_POINT('Ctrl Pts',(185.089626460494,4.59778811197941,337.236718862335));
#73738=CARTESIAN_POINT('Ctrl Pts',(184.904124633665,5.31167233335097,333.92231966833));
#73739=CARTESIAN_POINT('Ctrl Pts',(184.672259605103,2.91125672484798,329.972890248405));
#73740=CARTESIAN_POINT('Ctrl Pts',(184.394021570829,-2.66092683012348,329.831943356036));
#73741=CARTESIAN_POINT('Ctrl Pts',(184.115783536555,-5.78129223874898,334.4406109034));
#73742=CARTESIAN_POINT('Ctrl Pts',(183.837545502281,-3.60141999782881,339.559046781404));
#73743=CARTESIAN_POINT('Ctrl Pts',(183.559307468008,1.88614899471333,340.495592016401));
#73744=CARTESIAN_POINT('Ctrl Pts',(183.281069433733,5.64138409112437,336.387919992591));
#73745=CARTESIAN_POINT('Ctrl Pts',(183.00283139946,4.22036822806485,331.007100272962));
#73746=CARTESIAN_POINT('Ctrl Pts',(182.724593365185,-1.07402183899175,329.290227153788));
#73747=CARTESIAN_POINT('Ctrl Pts',(182.446355330911,-5.38258365553329,332.813275814337));
#73748=CARTESIAN_POINT('Ctrl Pts',(182.168117296638,-4.75174137159609,338.342970859998));
#73749=CARTESIAN_POINT('Ctrl Pts',(181.889879262364,0.239763929394143,340.804912264382));
#73750=CARTESIAN_POINT('Ctrl Pts',(181.61164122809,5.01120958425209,337.939749451869));
#73751=CARTESIAN_POINT('Ctrl Pts',(181.333403193816,5.18395902469876,332.376833562816));
#73752=CARTESIAN_POINT('Ctrl Pts',(181.055165159542,0.599456856430579,329.22115264934));
#73753=CARTESIAN_POINT('Ctrl Pts',(180.776927125268,-4.5351532933155,331.36863790884));
#73754=CARTESIAN_POINT('Ctrl Pts',(180.498689090994,-5.50792270834741,336.848568836761));
#73755=CARTESIAN_POINT('Ctrl Pts',(180.22045105672,-1.42615142470787,340.63209634096));
#73756=CARTESIAN_POINT('Ctrl Pts',(179.942213022446,3.96437726915641,339.247131679169));
#73757=CARTESIAN_POINT('Ctrl Pts',(179.663974988173,5.71685582915296,333.964637219027));
#73758=CARTESIAN_POINT('Ctrl Pts',(179.385736953898,2.22305997841688,329.632279765444));
#73759=CARTESIAN_POINT('Ctrl Pts',(179.107498919624,-3.31080509788334,330.225800015512));
#73760=CARTESIAN_POINT('Ctrl Pts',(178.82926088535,-5.80639325850615,335.200533086233));
#73761=CARTESIAN_POINT('Ctrl Pts',(178.551022851076,-2.97353999876288,339.991239923725));
#73762=CARTESIAN_POINT('Ctrl Pts',(178.272784816803,2.58808701297097,340.201559543127));
#73763=CARTESIAN_POINT('Ctrl Pts',(177.994546782528,5.77466478120961,335.638484750344));
#73764=CARTESIAN_POINT('Ctrl Pts',(177.716308748255,3.66191790929846,330.489481923198));
#73765=CARTESIAN_POINT('Ctrl Pts',(177.43807071398,-1.81131697585433,329.47971496158));
#73766=CARTESIAN_POINT('Ctrl Pts',(177.159832679707,-5.62233300847941,333.535832099607));
#73767=CARTESIAN_POINT('Ctrl Pts',(176.881594645433,-4.2738170240765,338.935594509187));
#73768=CARTESIAN_POINT('Ctrl Pts',(176.603356611159,0.996717761543614,340.723719926729));
#73769=CARTESIAN_POINT('Ctrl Pts',(176.325118576885,5.35257936910628,337.259272049606));
#73770=CARTESIAN_POINT('Ctrl Pts',(176.046880542611,4.79645789348621,331.721523559292));
#73771=CARTESIAN_POINT('Ctrl Pts',(175.768642508337,-0.161302195332879,
329.192384508421));
#73772=CARTESIAN_POINT('Ctrl Pts',(175.490404474063,-4.97103764033839,331.992808473886));
#73773=CARTESIAN_POINT('Ctrl Pts',(175.212166439789,-5.21892521518643,337.552887716805));
#73774=CARTESIAN_POINT('Ctrl Pts',(174.933928405515,-0.677482151275358,
340.770219582566));
#73775=CARTESIAN_POINT('Ctrl Pts',(174.655690371242,4.48567628324494,338.692306105712));
#73776=CARTESIAN_POINT('Ctrl Pts',(174.377452336967,5.53239580110267,333.226017813993));
#73777=CARTESIAN_POINT('Ctrl Pts',(174.099214302694,1.50211735031779,329.38768679044));
#73778=CARTESIAN_POINT('Ctrl Pts',(173.820976268419,-3.90663202163858,330.699692761692));
#73779=CARTESIAN_POINT('Ctrl Pts',(173.542738234146,-5.73032284913103,335.95802721311));
#73780=CARTESIAN_POINT('Ctrl Pts',(173.264500199872,-2.29538097740274,340.337194231514));
#73781=CARTESIAN_POINT('Ctrl Pts',(172.986262165598,3.24599813752044,339.818496880517));
#73782=CARTESIAN_POINT('Ctrl Pts',(172.708024131324,5.80857267249504,334.877936063166));
#73783=CARTESIAN_POINT('Ctrl Pts',(172.42978609705,3.04070580031311,330.049391518987));
#73784=CARTESIAN_POINT('Ctrl Pts',(172.151548062776,-2.51757190407213,329.763947306973));
#73785=CARTESIAN_POINT('Ctrl Pts',(171.873310028502,-5.76551103139077,334.283551367338));
#73786=CARTESIAN_POINT('Ctrl Pts',(171.595071994228,-3.72252578400546,339.460629763133));
#73787=CARTESIAN_POINT('Ctrl Pts',(171.316833959954,1.73656643097114,340.544254064088));
#73788=CARTESIAN_POINT('Ctrl Pts',(171.03859592568,5.60203726392403,336.539998243486));
#73789=CARTESIAN_POINT('Ctrl Pts',(170.760357891406,4.32660118570833,331.122508765173));
#73790=CARTESIAN_POINT('Ctrl Pts',(170.482119857132,-0.919292940103036,
329.263335761385));
#73791=CARTESIAN_POINT('Ctrl Pts',(170.203881822858,-5.32156550352343,332.668614856348));
#73792=CARTESIAN_POINT('Ctrl Pts',(169.925643788584,-4.84031595053847,338.213371686453));
#73793=CARTESIAN_POINT('Ctrl Pts',(169.64740575431,0.0828201073093179,340.809264749189));
#73794=CARTESIAN_POINT('Ctrl Pts',(169.369167720037,4.92995337510213,338.0740812962));
#73795=CARTESIAN_POINT('Ctrl Pts',(169.090929685762,5.25294119655625,332.517858811056));
#73796=CARTESIAN_POINT('Ctrl Pts',(168.812691651489,0.755382415215671,329.23946065866));
#73797=CARTESIAN_POINT('Ctrl Pts',(168.534453617214,-4.43537965914216,331.247424434392));
#73798=CARTESIAN_POINT('Ctrl Pts',(168.256215582941,-5.55585928640169,336.699071418756));
#73799=CARTESIAN_POINT('Ctrl Pts',(167.977977548667,-1.57780885087906,340.591505640382));
#73800=CARTESIAN_POINT('Ctrl Pts',(167.699739514393,3.8481734786748,339.352697666316));
#73801=CARTESIAN_POINT('Ctrl Pts',(167.421501480119,5.74274380579626,334.119483289585));
#73802=CARTESIAN_POINT('Ctrl Pts',(167.143263445845,2.3672829050982,329.694306101596));
#73803=CARTESIAN_POINT('Ctrl Pts',(166.865025411571,-3.18059857657007,330.138085892259));
#73804=CARTESIAN_POINT('Ctrl Pts',(166.586787377297,-5.80969169007805,335.043572497861));
#73805=CARTESIAN_POINT('Ctrl Pts',(166.308549343023,-3.10731649051019,339.909073265305));
#73806=CARTESIAN_POINT('Ctrl Pts',(166.030311308749,2.44659718848265,340.269589954981));
#73807=CARTESIAN_POINT('Ctrl Pts',(165.752073274475,5.75530473932027,335.794281721991));
#73808=CARTESIAN_POINT('Ctrl Pts',(165.473835240201,3.78245407904238,330.590072876309));
#73809=CARTESIAN_POINT('Ctrl Pts',(165.195597205928,-1.66149886064201,329.43278906162));
#73810=CARTESIAN_POINT('Ctrl Pts',(164.917359171654,-5.58071881959822,333.384452553184));
#73811=CARTESIAN_POINT('Ctrl Pts',(164.63912113738,-4.37859548908389,338.81868009125));
#73812=CARTESIAN_POINT('Ctrl Pts',(164.360883103105,0.841700293799237,340.748561273202));
#73813=CARTESIAN_POINT('Ctrl Pts',(164.082645068832,5.28958014053878,337.403072623362));
#73814=CARTESIAN_POINT('Ctrl Pts',(163.804407034558,4.88329036638077,331.852319696357));
#73815=CARTESIAN_POINT('Ctrl Pts',(163.526169000284,-0.00432289975708849,
329.19014652432));
#73816=CARTESIAN_POINT('Ctrl Pts',(163.24793096601,-4.8879691045938,331.859590133619));
#73817=CARTESIAN_POINT('Ctrl Pts',(162.969692931736,-5.28599820845056,337.410941524921));
#73818=CARTESIAN_POINT('Ctrl Pts',(162.691454897462,-0.833144777617896,
340.749807464242));
#73819=CARTESIAN_POINT('Ctrl Pts',(162.413216863188,4.38427331843794,338.812159960648));
#73820=CARTESIAN_POINT('Ctrl Pts',(162.134978828914,5.5783085019314,333.376149528555));
#73821=CARTESIAN_POINT('Ctrl Pts',(161.85674079464,1.65321230890092,329.430322706114));
#73822=CARTESIAN_POINT('Ctrl Pts',(161.578502760366,-3.78901241863424,330.59570652797));
#73823=CARTESIAN_POINT('Ctrl Pts',(161.300264726092,-5.75411637532039,335.802845461843));
#73824=CARTESIAN_POINT('Ctrl Pts',(161.022026691818,-2.43875266499349,340.273224965362));
#73825=CARTESIAN_POINT('Ctrl Pts',(160.743788657544,3.1146183700676,339.904443750842));
#73826=CARTESIAN_POINT('Ctrl Pts',(160.465550623271,5.80975009860945,335.034926895645));
#73827=CARTESIAN_POINT('Ctrl Pts',(160.187312588997,3.17335991342832,330.133358143835));
#73828=CARTESIAN_POINT('Ctrl Pts',(159.909074554723,-2.37517582559034,329.697834791912));
#73829=CARTESIAN_POINT('Ctrl Pts',(159.630836520449,-5.74404776700253,334.128030191621));
#73830=CARTESIAN_POINT('Ctrl Pts',(159.352598486175,-3.84169185464261,339.358419414226));
#73831=CARTESIAN_POINT('Ctrl Pts',(159.074360451901,1.58612796944403,340.589151470561));
#73832=CARTESIAN_POINT('Ctrl Pts',(158.796122417627,5.55838156718232,336.690801718102));
#73833=CARTESIAN_POINT('Ctrl Pts',(158.517884383353,4.42979044229486,331.240828185134));
#73834=CARTESIAN_POINT('Ctrl Pts',(158.239646349079,-0.763953987886848,
329.240591141382));
#73835=CARTESIAN_POINT('Ctrl Pts',(157.961408314805,-5.25662911932717,332.525678598449));
#73836=CARTESIAN_POINT('Ctrl Pts',(157.683170280531,-4.92537329567956,338.081414284795));
#73837=CARTESIAN_POINT('Ctrl Pts',(157.404932246257,-0.0741750969775079,
340.809381563585));
#73838=CARTESIAN_POINT('Ctrl Pts',(157.126694211983,4.84509249339818,338.206165127804));
#73839=CARTESIAN_POINT('Ctrl Pts',(156.848456177709,5.31809021603033,332.660698277158));
#73840=CARTESIAN_POINT('Ctrl Pts',(156.570218143435,0.910755042294368,329.261974089526));
#73841=CARTESIAN_POINT('Ctrl Pts',(156.291980109161,-4.33236659103269,331.128951586813));
#73842=CARTESIAN_POINT('Ctrl Pts',(156.013742074888,-5.59973934939517,336.548333076301));
#73843=CARTESIAN_POINT('Ctrl Pts',(155.735504040614,-1.72831395883512,340.546832155026));
#73844=CARTESIAN_POINT('Ctrl Pts',(155.457266006339,3.72915964187575,339.455085236193));
#73845=CARTESIAN_POINT('Ctrl Pts',(155.179027972066,5.76443848154334,334.274972353055));
#73846=CARTESIAN_POINT('Ctrl Pts',(154.900789937792,2.50977720967112,329.760206640129));
#73847=CARTESIAN_POINT('Ctrl Pts',(154.622551903518,-3.04806956326539,330.053921954334));
#73848=CARTESIAN_POINT('Ctrl Pts',(154.344313869244,-5.80874788742625,334.886580087053));
#73849=CARTESIAN_POINT('Ctrl Pts',(154.06607583497,-3.23882401227433,339.82332199981));
#73850=CARTESIAN_POINT('Ctrl Pts',(153.787837800696,2.3033208539777,340.333772505456));
#73851=CARTESIAN_POINT('Ctrl Pts',(153.509599766422,5.73174216949446,335.949498709199));
#73852=CARTESIAN_POINT('Ctrl Pts',(153.231361732148,3.90022829644191,330.693883962088));
#73853=CARTESIAN_POINT('Ctrl Pts',(152.953123697874,-1.5104675169801,329.3899283448));
#73854=CARTESIAN_POINT('Ctrl Pts',(152.6748856636,-5.53502958453341,333.234252680968));
#73855=CARTESIAN_POINT('Ctrl Pts',(152.396647629326,-4.48017669926329,338.698977269423));
#73856=CARTESIAN_POINT('Ctrl Pts',(152.118409595052,0.686068215621029,340.769205014545));
#73857=CARTESIAN_POINT('Ctrl Pts',(151.840171560778,5.22271845538023,337.545118471145));
#73858=CARTESIAN_POINT('Ctrl Pts',(151.561933526504,4.96655705583505,331.985414272663));
#73859=CARTESIAN_POINT('Ctrl Pts',(151.283695492231,0.152659552412012,329.192150900945));
#73860=CARTESIAN_POINT('Ctrl Pts',(151.005457457957,-4.80133136900823,331.728664923719));
#73861=CARTESIAN_POINT('Ctrl Pts',(150.727219423682,-5.34921136062445,337.267234861169));
#73862=CARTESIAN_POINT('Ctrl Pts',(150.448981389409,-0.988199040825888,
340.725196830856));
#73863=CARTESIAN_POINT('Ctrl Pts',(150.170743355135,4.27966895294467,338.929230172633));
#73864=CARTESIAN_POINT('Ctrl Pts',(149.892505320861,5.62014791640809,333.527466980328));
#73865=CARTESIAN_POINT('Ctrl Pts',(149.614267286587,1.80310009023112,329.477025605624));
#73866=CARTESIAN_POINT('Ctrl Pts',(149.336029252313,-3.66862607503718,330.49493631367));
#73867=CARTESIAN_POINT('Ctrl Pts',(149.057791218039,-5.77370824007606,335.647077472031));
#73868=CARTESIAN_POINT('Ctrl Pts',(148.779553183765,-2.5803435729911,340.205405185156));
#73869=CARTESIAN_POINT('Ctrl Pts',(148.501315149491,2.98096430521908,339.986809391519));
#73870=CARTESIAN_POINT('Ctrl Pts',(148.223077115217,5.80668523949074,335.191892224471));
#73871=CARTESIAN_POINT('Ctrl Pts',(147.944839080943,3.30369683601538,330.22087839535));
#73872=CARTESIAN_POINT('Ctrl Pts',(147.666601046669,-2.23104539138592,329.635593923097));
#73873=CARTESIAN_POINT('Ctrl Pts',(147.388363012396,-5.71839019328836,333.973145729115));
#73874=CARTESIAN_POINT('Ctrl Pts',(147.110124978121,-3.95805271811097,339.25302654318));
#73875=CARTESIAN_POINT('Ctrl Pts',(146.831886943848,1.43453131571451,340.629967673136));
#73876=CARTESIAN_POINT('Ctrl Pts',(146.553648909573,5.5106671347563,336.840370567645));
#73877=CARTESIAN_POINT('Ctrl Pts',(146.2754108753,4.52974506154582,331.361892556048));
#73878=CARTESIAN_POINT('Ctrl Pts',(145.997172841026,-0.608057195717691,
329.222052047391));
#73879=CARTESIAN_POINT('Ctrl Pts',(145.718934806752,-5.18785433938055,332.38454909247));
#73880=CARTESIAN_POINT('Ctrl Pts',(145.440696772478,-5.00683412839853,337.947206831397));
#73881=CARTESIAN_POINT('Ctrl Pts',(145.162458738204,-0.231116138535769,
340.805256361854));
#73882=CARTESIAN_POINT('Ctrl Pts',(144.88422070393,4.75669372039265,338.33590781448));
#73883=CARTESIAN_POINT('Ctrl Pts',(144.605982669656,5.37935596080095,332.805245903677));
#73884=CARTESIAN_POINT('Ctrl Pts',(144.327744635382,1.06546263514606,329.288677432552));
#73885=CARTESIAN_POINT('Ctrl Pts',(144.049506601108,-4.22619002457966,331.013305382591));
#73886=CARTESIAN_POINT('Ctrl Pts',(143.771268566834,-5.63953047721114,336.396464139511));
#73887=CARTESIAN_POINT('Ctrl Pts',(143.49303053256,-1.87755705023934,340.498108367378));
#73888=CARTESIAN_POINT('Ctrl Pts',(143.214792498286,3.60742276904044,339.554219698449));
#73889=CARTESIAN_POINT('Ctrl Pts',(142.936554464012,5.78192395864463,334.430990832426));
#73890=CARTESIAN_POINT('Ctrl Pts',(142.658316429739,2.65043887245836,329.829933280924));
#73891=CARTESIAN_POINT('Ctrl Pts',(142.380078395464,-2.91331484656925,329.973369647459));
#73892=CARTESIAN_POINT('Ctrl Pts',(142.101840361191,-5.80356253135695,334.729670495578));
#73893=CARTESIAN_POINT('Ctrl Pts',(141.823602326917,-3.36796654156104,339.734048739849));
#73894=CARTESIAN_POINT('Ctrl Pts',(141.545364292643,2.1583626323208,340.394060330005));
#73895=CARTESIAN_POINT('Ctrl Pts',(141.267126258369,5.70399427590206,336.104022371516));
#73896=CARTESIAN_POINT('Ctrl Pts',(140.988888224095,4.0151545633055,330.80083937803));
#73897=CARTESIAN_POINT('Ctrl Pts',(140.710650189821,-1.3583332284523,329.351164107817));
#73898=CARTESIAN_POINT('Ctrl Pts',(140.432412155547,-5.48529866542502,333.085342159178));
#73899=CARTESIAN_POINT('Ctrl Pts',(140.154174121273,-4.57848648001278,338.576573450759));
#73900=CARTESIAN_POINT('Ctrl Pts',(139.875936086999,0.529935169757505,340.785636076714));
#73901=CARTESIAN_POINT('Ctrl Pts',(139.597698052725,5.15204313607163,337.685305870919));
#73902=CARTESIAN_POINT('Ctrl Pts',(139.319460018451,5.04619716044484,332.120710102429));
#73903=CARTESIAN_POINT('Ctrl Pts',(139.041221984177,0.309530532425838,329.198396174692));
#73904=CARTESIAN_POINT('Ctrl Pts',(138.762983949904,-4.71118769653721,331.600128445908));
#73905=CARTESIAN_POINT('Ctrl Pts',(138.484745915629,-5.40851851340445,337.121872660291));
#73906=CARTESIAN_POINT('Ctrl Pts',(138.206507881356,-1.14253172012296,340.696405653115));
#73907=CARTESIAN_POINT('Ctrl Pts',(137.928269847081,4.17193956897484,339.043431256885));
#73908=CARTESIAN_POINT('Ctrl Pts',(137.650031812808,5.65788349335158,333.679859677159));
#73909=CARTESIAN_POINT('Ctrl Pts',(137.371793778534,1.95167124610305,329.527761386465));
#73910=CARTESIAN_POINT('Ctrl Pts',(137.09355574426,-3.54556089707387,330.397455701302));
#73911=CARTESIAN_POINT('Ctrl Pts',(136.815317709986,-5.78908413739917,335.490836985613));
#73912=CARTESIAN_POINT('Ctrl Pts',(136.537079675712,-2.72005031157503,340.133784412968));
#73913=CARTESIAN_POINT('Ctrl Pts',(136.258841641438,2.84513353730471,340.065533659077));
#73914=CARTESIAN_POINT('Ctrl Pts',(135.980603607164,5.7993803331021,335.348717433405));
#73915=CARTESIAN_POINT('Ctrl Pts',(135.70236557289,3.4316213959251,330.311888366159));
#73916=CARTESIAN_POINT('Ctrl Pts',(135.424127538616,-2.08528584564359,329.577270148875));
#73917=CARTESIAN_POINT('Ctrl Pts',(135.145889504342,-5.68855704543379,333.819011076606));
#73918=CARTESIAN_POINT('Ctrl Pts',(134.867651470068,-4.07152340759375,339.14452810797));
#73919=CARTESIAN_POINT('Ctrl Pts',(134.589413435794,1.28188716580795,340.666672867782));
#73920=CARTESIAN_POINT('Ctrl Pts',(134.31117540152,5.45892880777134,336.988595576787));
#73921=CARTESIAN_POINT('Ctrl Pts',(134.032937367246,4.62639205650012,331.485613476596));
#73922=CARTESIAN_POINT('Ctrl Pts',(133.754699332972,-0.451716399586434,
329.207732016673));
#73923=CARTESIAN_POINT('Ctrl Pts',(133.476461298699,-5.11529138309565,332.245329391314));
#73924=CARTESIAN_POINT('Ctrl Pts',(133.198223264425,-5.08463896591503,337.810847324675));
#73925=CARTESIAN_POINT('Ctrl Pts',(132.919985230151,-0.38788841886232,340.79689215622));
#73926=CARTESIAN_POINT('Ctrl Pts',(132.641747195877,4.66482160495669,338.46321461799));
#73927=CARTESIAN_POINT('Ctrl Pts',(132.363509161603,5.43669369456094,332.951396141795));
#73928=CARTESIAN_POINT('Ctrl Pts',(132.085271127329,1.21939222613404,329.319551188931));
#73929=CARTESIAN_POINT('Ctrl Pts',(131.807033093055,-4.11692749001633,330.900570266698));
#73930=CARTESIAN_POINT('Ctrl Pts',(131.528795058781,-5.67520361432885,336.243575503233));
#73931=CARTESIAN_POINT('Ctrl Pts',(131.250557024507,-2.02542914763983,340.445369855595));
#73932=CARTESIAN_POINT('Ctrl Pts',(130.972318990233,3.483051752553,339.650028665005));
#73933=CARTESIAN_POINT('Ctrl Pts',(130.694080955959,5.79518746918758,334.587424802851));
#73934=CARTESIAN_POINT('Ctrl Pts',(130.415842921685,2.78916518217566,329.903435109521));
#73935=CARTESIAN_POINT('Ctrl Pts',(130.137604887411,-2.77643282450829,329.896487791008));
#73936=CARTESIAN_POINT('Ctrl Pts',(129.859366853137,-5.7941394082223,334.572958298972));
#73937=CARTESIAN_POINT('Ctrl Pts',(129.581128818863,-3.49464977836818,339.641318672843));
#73938=CARTESIAN_POINT('Ctrl Pts',(129.302890784589,2.01182837214824,340.450409406398));
#73939=CARTESIAN_POINT('Ctrl Pts',(129.024652750315,5.67208132008231,336.257739875612));
#73940=CARTESIAN_POINT('Ctrl Pts',(128.746414716042,4.1271489603599,330.910861025188));
#73941=CARTESIAN_POINT('Ctrl Pts',(128.468176681768,-1.20520708366599,329.316524656355));
#73942=CARTESIAN_POINT('Ctrl Pts',(128.189938647494,-5.43156237583899,332.937829722429));
#73943=CARTESIAN_POINT('Ctrl Pts',(127.91170061322,-4.67345304543382,338.451558014644));
#73944=CARTESIAN_POINT('Ctrl Pts',(127.633462578946,0.373415164712107,340.797842461735));
#73945=CARTESIAN_POINT('Ctrl Pts',(127.355224544672,5.07760578980047,337.823532457706));
#73946=CARTESIAN_POINT('Ctrl Pts',(127.076986510398,5.12215252692763,332.258108392511));
#73947=CARTESIAN_POINT('Ctrl Pts',(126.798748476124,0.466175492940766,329.208877785255));
#73948=CARTESIAN_POINT('Ctrl Pts',(126.52051044185,-4.61760391017891,331.474074557648));
#73949=CARTESIAN_POINT('Ctrl Pts',(126.242272407576,-5.46387636064937,336.974961065912));
#73950=CARTESIAN_POINT('Ctrl Pts',(125.964034373302,-1.29603012163481,340.663454954368));
#73951=CARTESIAN_POINT('Ctrl Pts',(125.685796339028,4.06116383063079,339.154679823657));
#73952=CARTESIAN_POINT('Ctrl Pts',(125.407558304754,5.69148767820639,333.833216341752));
#73953=CARTESIAN_POINT('Ctrl Pts',(125.12932027048,2.09881728971241,329.58249300132));
#73954=CARTESIAN_POINT('Ctrl Pts',(124.851082236206,-3.41990674705822,330.303335871306));
#73955=CARTESIAN_POINT('Ctrl Pts',(124.572844201933,-5.80023283979438,335.334238089545));
#73956=CARTESIAN_POINT('Ctrl Pts',(124.294606167658,-2.85777086674761,340.058414946355));
#73957=CARTESIAN_POINT('Ctrl Pts',(124.016368133385,2.70722525008458,340.140559068977));
#73958=CARTESIAN_POINT('Ctrl Pts',(123.738130099111,5.78784071349336,335.505288008526));
#73959=CARTESIAN_POINT('Ctrl Pts',(123.459892064837,3.55704018251817,330.406321600691));
#73960=CARTESIAN_POINT('Ctrl Pts',(123.181654030563,-1.93800362212678,329.522906057319));
#73961=CARTESIAN_POINT('Ctrl Pts',(122.903415996289,-5.65457010763266,333.665738783371));
#73962=CARTESIAN_POINT('Ctrl Pts',(122.625177962015,-4.18202106668204,339.033003334261));
#73963=CARTESIAN_POINT('Ctrl Pts',(122.346939927741,1.12830698063291,340.699240252331));
#73964=CARTESIAN_POINT('Ctrl Pts',(122.068701893467,5.40320436560478,337.135368511485));
#73965=CARTESIAN_POINT('Ctrl Pts',(121.790463859193,4.71966085542685,331.611900605637));
#73966=CARTESIAN_POINT('Ctrl Pts',(121.512225824919,-0.295045759696265,
329.197641505731));
#73967=CARTESIAN_POINT('Ctrl Pts',(121.233987790645,-5.03899323601439,332.108121153345));
#73968=CARTESIAN_POINT('Ctrl Pts',(120.955749756371,-5.15873099506036,337.672435334473));
#73969=CARTESIAN_POINT('Ctrl Pts',(120.677511722097,-0.544377462684104,
340.784295054235));
#73970=CARTESIAN_POINT('Ctrl Pts',(120.399273687823,4.56954323219917,338.587992578782));
#73971=CARTESIAN_POINT('Ctrl Pts',(120.12103565355,5.49006154924083,333.099042272464));
#73972=CARTESIAN_POINT('Ctrl Pts',(119.842797619276,1.37243141571984,329.354572814616));
#73973=CARTESIAN_POINT('Ctrl Pts',(119.564559585002,-4.00465877095267,330.790828558426));
#73974=CARTESIAN_POINT('Ctrl Pts',(119.286321550728,-5.7067327121886,336.089778806901));
#73975=CARTESIAN_POINT('Ctrl Pts',(119.008083516454,-2.17182227468582,340.388655129391));
#73976=CARTESIAN_POINT('Ctrl Pts',(118.72984548218,3.35613740825191,339.742442176059));
#73977=CARTESIAN_POINT('Ctrl Pts',(118.451607447906,5.80421932814381,334.744160036089));
#73978=CARTESIAN_POINT('Ctrl Pts',(118.173369413632,2.92585484073498,329.980658454809));
#73979=CARTESIAN_POINT('Ctrl Pts',(117.895131379358,-2.63752344846967,329.823332524191));
#73980=CARTESIAN_POINT('Ctrl Pts',(117.616893345084,-5.780485398796,334.416557928635));
#73981=CARTESIAN_POINT('Ctrl Pts',(117.33865531081,-3.61878121847186,339.545199510381));
#73982=CARTESIAN_POINT('Ctrl Pts',(117.060417276536,1.86382507292066,340.502778588485));
#73983=CARTESIAN_POINT('Ctrl Pts',(116.782179242262,5.63602660490689,336.410538976814));
#73984=CARTESIAN_POINT('Ctrl Pts',(116.503941207988,4.23612970918638,331.023868565644));
#73985=CARTESIAN_POINT('Ctrl Pts',(116.225703173714,-1.05120089548245,329.286035284177));
#73986=CARTESIAN_POINT('Ctrl Pts',(115.94746513944,-5.37385995406682,332.791823084441));
#73987=CARTESIAN_POINT('Ctrl Pts',(115.669227105167,-4.76500705084698,338.324022247475));
#73988=CARTESIAN_POINT('Ctrl Pts',(115.390989070892,0.216622491546355,340.80581525649));
#73989=CARTESIAN_POINT('Ctrl Pts',(115.112751036619,4.99946077079033,337.959697298317));
#73990=CARTESIAN_POINT('Ctrl Pts',(114.834513002344,5.19436769260004,332.397508814538));
#73991=CARTESIAN_POINT('Ctrl Pts',(114.556274968071,0.622480051652159,329.223588078952));
#73992=CARTESIAN_POINT('Ctrl Pts',(114.278036933797,-4.52064834490641,331.350595303611));
#73993=CARTESIAN_POINT('Ctrl Pts',(113.999798899523,-5.51524448000453,336.826607353021));
#73994=CARTESIAN_POINT('Ctrl Pts',(113.721560865249,-1.44858216067782,340.626368795244));
#73995=CARTESIAN_POINT('Ctrl Pts',(113.443322830975,3.94742262646529,339.26289463914));
#73996=CARTESIAN_POINT('Ctrl Pts',(113.165084796701,5.72093593316378,333.987424992917));
#73997=CARTESIAN_POINT('Ctrl Pts',(112.886846762427,2.24443077487382,329.641180485114));
#73998=CARTESIAN_POINT('Ctrl Pts',(112.608608728153,-3.2917553777739,330.212645550074));
#73999=CARTESIAN_POINT('Ctrl Pts',(112.330370693879,-5.80714620646826,335.177395132495));
#74000=CARTESIAN_POINT('Ctrl Pts',(112.052132659606,-2.99340467482419,339.979351820174));
#74001=CARTESIAN_POINT('Ctrl Pts',(111.773894625331,2.56734014432545,340.211830837592));
#74002=CARTESIAN_POINT('Ctrl Pts',(111.495656591058,5.77207480690603,335.661489621848));
#74003=CARTESIAN_POINT('Ctrl Pts',(111.217418556783,3.67986161487345,330.504109143706));
#74004=CARTESIAN_POINT('Ctrl Pts',(110.93918052251,-1.78930626646011,329.472541345144));
#74005=CARTESIAN_POINT('Ctrl Pts',(110.660942488236,-5.61645419718042,333.513440768989));
#74006=CARTESIAN_POINT('Ctrl Pts',(110.382704453962,-4.28946500987634,338.918533657553));
#74007=CARTESIAN_POINT('Ctrl Pts',(110.104466419688,0.973902904591502,340.727646046044));
#74008=CARTESIAN_POINT('Ctrl Pts',(109.826228385414,5.34353449829903,337.280582197997));
#74009=CARTESIAN_POINT('Ctrl Pts',(109.54799035114,4.80948335335744,331.740661728187));
#74010=CARTESIAN_POINT('Ctrl Pts',(109.269752316866,-0.138159677102331,
329.191787882665));
#74011=CARTESIAN_POINT('Ctrl Pts',(108.991514282592,-4.95901561111879,331.973024568152));
#74012=CARTESIAN_POINT('Ctrl Pts',(108.713276248318,-5.22905611376197,337.532071929362));
#74013=CARTESIAN_POINT('Ctrl Pts',(108.435038214044,-0.700469001547521,
340.767474254316));
#74014=CARTESIAN_POINT('Ctrl Pts',(108.15680017977,4.47092817448158,338.710150583865));
#74015=CARTESIAN_POINT('Ctrl Pts',(107.878562145496,5.53942055558062,333.248076484335));
#74016=CARTESIAN_POINT('Ctrl Pts',(107.600324111222,1.52446845453669,329.39371673678));
#74017=CARTESIAN_POINT('Ctrl Pts',(107.322086076948,-3.88946584611805,330.684160391279));
#74018=CARTESIAN_POINT('Ctrl Pts',(107.043848042674,-5.73409474821204,335.935186353011));
#74019=CARTESIAN_POINT('Ctrl Pts',(106.7656100084,-2.31662953497166,340.328005601914));
#74020=CARTESIAN_POINT('Ctrl Pts',(106.487371974127,3.22677240911617,339.831392751173));
#74021=CARTESIAN_POINT('Ctrl Pts',(106.209133939853,5.80901294044096,334.901082083922));
#74022=CARTESIAN_POINT('Ctrl Pts',(105.930895905579,3.06040803721359,330.061546928227));
#74023=CARTESIAN_POINT('Ctrl Pts',(105.652657871305,-2.49668815021611,329.753957265053));
#74024=CARTESIAN_POINT('Ctrl Pts',(105.374419837031,-5.76261047324917,334.260583588273));
#74025=CARTESIAN_POINT('Ctrl Pts',(105.096181802757,-3.74027022097263,339.445761438768));
#74026=CARTESIAN_POINT('Ctrl Pts',(104.817943768483,1.71446080679252,340.551129636237));
#74027=CARTESIAN_POINT('Ctrl Pts',(104.539705734209,5.59585645756422,336.56230810107));
#74028=CARTESIAN_POINT('Ctrl Pts',(104.261467699935,4.34201723193514,331.139779481181));
#74029=CARTESIAN_POINT('Ctrl Pts',(103.983229665661,-0.896427119371509,
329.259718254652));
#74030=CARTESIAN_POINT('Ctrl Pts',(103.704991631387,-5.31223353447353,332.647428859408));
#74031=CARTESIAN_POINT('Ctrl Pts',(103.426753597113,-4.85308164342763,338.194059275994));
#74032=CARTESIAN_POINT('Ctrl Pts',(103.148515562839,0.0596716404241646,
340.809548639237));
#74033=CARTESIAN_POINT('Ctrl Pts',(102.870277528565,4.91766514061068,338.093700965052));
#74034=CARTESIAN_POINT('Ctrl Pts',(102.592039494291,5.26278992587726,332.538809578187));
#74035=CARTESIAN_POINT('Ctrl Pts',(102.313801460018,0.778330074818259,329.242516314312));
#74036=CARTESIAN_POINT('Ctrl Pts',(102.035563425744,-4.42039179776838,331.22978084847));
#74037=CARTESIAN_POINT('Ctrl Pts',(101.75732539147,-5.56258536241897,336.676919849645));
#74038=CARTESIAN_POINT('Ctrl Pts',(101.479087357196,-1.60007644360303,340.585174256096));
#74039=CARTESIAN_POINT('Ctrl Pts',(101.200849322922,3.83079901041782,339.367996684764));
#74040=CARTESIAN_POINT('Ctrl Pts',(100.922611288648,5.74620675507894,334.14237302735));
#74041=CARTESIAN_POINT('Ctrl Pts',(100.644373254374,2.3884053744768,329.703780984183));
#74042=CARTESIAN_POINT('Ctrl Pts',(100.3661352201,-3.16120036547716,330.125450959766));
#74043=CARTESIAN_POINT('Ctrl Pts',(100.087897185826,-5.80981918927364,335.020422641347));
#74044=CARTESIAN_POINT('Ctrl Pts',(99.809659151552,-3.12685269586437,339.8966527664));
#74045=CARTESIAN_POINT('Ctrl Pts',(99.531421117278,2.4255803642695,340.279296922205));
#74046=CARTESIAN_POINT('Ctrl Pts',(99.2531830830042,5.75209412562066,335.817208214797));
#74047=CARTESIAN_POINT('Ctrl Pts',(98.9749450487301,3.79999600866009,330.605179590644));
#74048=CARTESIAN_POINT('Ctrl Pts',(98.6967070144562,-1.6393023575986,329.426212788713));
#74049=CARTESIAN_POINT('Ctrl Pts',(98.4184689801823,-5.57423714635231,333.362228241617));
#74050=CARTESIAN_POINT('Ctrl Pts',(98.1402309459082,-4.39377678150391,338.801202663717));
#74051=CARTESIAN_POINT('Ctrl Pts',(97.8619929116345,0.818787683691637,340.751869506984));
#74052=CARTESIAN_POINT('Ctrl Pts',(97.5837548773604,5.27996277684976,337.424130601146));
#74053=CARTESIAN_POINT('Ctrl Pts',(97.3055168430865,4.89579396181571,331.871802822746));
#74054=CARTESIAN_POINT('Ctrl Pts',(97.0272788088127,0.0188272898237993,
329.190175421797));
#74055=CARTESIAN_POINT('Ctrl Pts',(96.7490407745384,-4.87541690814907,331.840138283395));
#74056=CARTESIAN_POINT('Ctrl Pts',(96.4708027402649,-5.29556297054915,337.389859602839));
#74057=CARTESIAN_POINT('Ctrl Pts',(96.1925647059907,-0.856049057257586,
340.746442039027));
#74058=CARTESIAN_POINT('Ctrl Pts',(95.9143266717167,4.36904844061587,338.829599433346));
#74059=CARTESIAN_POINT('Ctrl Pts',(95.636088637443,5.58473467158543,333.398389952479));
#74060=CARTESIAN_POINT('Ctrl Pts',(95.3578506031688,1.67539232498966,329.436954372495));
#74061=CARTESIAN_POINT('Ctrl Pts',(95.0796125688951,-3.77143282949893,330.580643654456));
#74062=CARTESIAN_POINT('Ctrl Pts',(94.8013745346211,-5.75726974261368,335.779911025129));
#74063=CARTESIAN_POINT('Ctrl Pts',(94.5231365003471,-2.45974519009395,340.263465559509));
#74064=CARTESIAN_POINT('Ctrl Pts',(94.2448984660733,3.0950512175955,339.916815438554));
#74065=CARTESIAN_POINT('Ctrl Pts',(93.9666604317991,5.80956480577865,335.058076361713));
#74066=CARTESIAN_POINT('Ctrl Pts',(93.6884223975253,3.19272652073472,330.146041464936));
#74067=CARTESIAN_POINT('Ctrl Pts',(93.4101843632514,-2.35402976782128,329.688412671475));
#74068=CARTESIAN_POINT('Ctrl Pts',(93.1319463289774,-5.7405276838701,334.105149170503));
#74069=CARTESIAN_POINT('Ctrl Pts',(92.8537082947034,-3.85902807448106,339.343077067782));
#74070=CARTESIAN_POINT('Ctrl Pts',(92.5754702604298,1.56384463969824,340.595427243672));
#74071=CARTESIAN_POINT('Ctrl Pts',(92.2972322261555,5.55160021033551,336.712936426414));
#74072=CARTESIAN_POINT('Ctrl Pts',(92.0189941918818,4.44473420943266,331.258509133536));
#74073=CARTESIAN_POINT('Ctrl Pts',(91.7407561576076,-0.740998771297037,
329.237592784498));
#74074=CARTESIAN_POINT('Ctrl Pts',(91.4625181233339,-5.24672811673134,332.504752484135));
#74075=CARTESIAN_POINT('Ctrl Pts',(91.18428008906,-4.93761251102159,338.061763999288));
#74076=CARTESIAN_POINT('Ctrl Pts',(90.9060420547858,-0.0973227829885132,
340.809039883857));
#74077=CARTESIAN_POINT('Ctrl Pts',(90.6278040205122,4.83227862651119,338.225445608299));
#74078=CARTESIAN_POINT('Ctrl Pts',(90.3495659862381,5.3273692647772,332.681907505503));
#74079=CARTESIAN_POINT('Ctrl Pts',(90.0713279519642,0.933611760598616,329.26564866992));
#74080=CARTESIAN_POINT('Ctrl Pts',(89.7930899176902,-4.31690747619431,331.111719411062));
#74081=CARTESIAN_POINT('Ctrl Pts',(89.5148518834163,-5.60586443953363,336.526007857746));
#74082=CARTESIAN_POINT('Ctrl Pts',(89.2366138491423,-1.75040234913642,340.539901417215));
#74083=CARTESIAN_POINT('Ctrl Pts',(88.9583758148684,3.71137814116694,339.469909214918));
#74084=CARTESIAN_POINT('Ctrl Pts',(88.6801377805944,5.767281691173,334.29794730184));
#74085=CARTESIAN_POINT('Ctrl Pts',(88.4018997463205,2.5306359581278,329.770248787585));
#74086=CARTESIAN_POINT('Ctrl Pts',(88.1236617120466,-3.02833704156575,330.041815769961));
#74087=CARTESIAN_POINT('Ctrl Pts',(87.8454236777727,-5.80824983639588,334.863435237565));
#74088=CARTESIAN_POINT('Ctrl Pts',(87.5671856434985,-3.25801748599256,339.810378171963));
#74089=CARTESIAN_POINT('Ctrl Pts',(87.2889476092249,2.28204942304687,340.342908059017));
#74090=CARTESIAN_POINT('Ctrl Pts',(87.0107095749507,5.72791325955045,335.972330081504));
#74091=CARTESIAN_POINT('Ctrl Pts',(86.732471540677,3.91735564162572,330.709459139764));
#74092=CARTESIAN_POINT('Ctrl Pts',(86.4542335064028,-1.48810142854445,329.383954217183));
#74093=CARTESIAN_POINT('Ctrl Pts',(86.1759954721289,-5.52794978208046,333.212211616794));
#74094=CARTESIAN_POINT('Ctrl Pts',(85.8977574378551,-4.49488021300627,338.681096027959));
#74095=CARTESIAN_POINT('Ctrl Pts',(85.6195194035811,0.66307458322058,340.771892947156));
#74096=CARTESIAN_POINT('Ctrl Pts',(85.3412813693072,5.2125356213907,337.565908901747));
#74097=CARTESIAN_POINT('Ctrl Pts',(85.0630433350333,4.97852965671024,332.005228129959));
#74098=CARTESIAN_POINT('Ctrl Pts',(84.7848053007592,0.175800509044065,329.192805300547));
#74099=CARTESIAN_POINT('Ctrl Pts',(84.5065672664855,-4.78825817096059,331.70955933277));
#74100=CARTESIAN_POINT('Ctrl Pts',(84.2283292322114,-5.35820300204945,337.245902198485));
#74101=CARTESIAN_POINT('Ctrl Pts',(83.9500911979375,-1.01100402510444,340.721213766112));
#74102=CARTESIAN_POINT('Ctrl Pts',(83.6718531636636,4.26397842328399,338.946251905556));
#74103=CARTESIAN_POINT('Ctrl Pts',(83.3936151293895,5.62597080884317,333.549872917852));
#74104=CARTESIAN_POINT('Ctrl Pts',(83.1153770951157,1.82509282231999,329.484254149597));
#74105=CARTESIAN_POINT('Ctrl Pts',(82.8371390608417,-3.65064590892035,330.480353935979));
#74106=CARTESIAN_POINT('Ctrl Pts',(82.5589010265678,-5.77624077298977,335.624066205448));
#74107=CARTESIAN_POINT('Ctrl Pts',(82.2806629922939,-2.60106473686054,340.195082129379));
#74108=CARTESIAN_POINT('Ctrl Pts',(82.0024249580199,2.96107001663303,339.998647862465));
#74109=CARTESIAN_POINT('Ctrl Pts',(81.7241869237459,5.80587452118426,335.215028232089));
#74110=CARTESIAN_POINT('Ctrl Pts',(81.4459488894722,3.32271367221217,330.234080366935));
#74111=CARTESIAN_POINT('Ctrl Pts',(81.167710855198,-2.20965247057562,329.626746604187));
#74112=CARTESIAN_POINT('Ctrl Pts',(80.8894728209243,-5.71425315553317,333.950368173687));
#74113=CARTESIAN_POINT('Ctrl Pts',(80.6112347866501,-3.97496806189624,339.237221377653));
#74114=CARTESIAN_POINT('Ctrl Pts',(80.3329967523764,1.41208655171044,340.635639064632));
#74115=CARTESIAN_POINT('Ctrl Pts',(80.0547587181022,5.5032901791758,336.862313963896));
#74116=CARTESIAN_POINT('Ctrl Pts',(79.7765206838285,4.54420563764141,331.3799708262));
#74117=CARTESIAN_POINT('Ctrl Pts',(79.4982826495544,-0.58502934519122,329.219675029759));
#74118=CARTESIAN_POINT('Ctrl Pts',(79.2200446152804,-5.17739153296086,332.36389814105));
#74119=CARTESIAN_POINT('Ctrl Pts',(78.9418065810067,-5.01853792910607,337.927233019501));
#74120=CARTESIAN_POINT('Ctrl Pts',(78.6635685467325,-0.25424614120906,340.804289361844));
#74121=CARTESIAN_POINT('Ctrl Pts',(78.3853305124589,4.74336357780861,338.354835027994));
#74122=CARTESIAN_POINT('Ctrl Pts',(78.1070924781846,5.38805855340297,332.826698106237));
#74123=CARTESIAN_POINT('Ctrl Pts',(77.828854443911,1.0882117221533,329.292968254504));
#74124=CARTESIAN_POINT('Ctrl Pts',(77.5506164096369,-4.21027094453775,330.996497199962));
#74125=CARTESIAN_POINT('Ctrl Pts',(77.272378375363,-5.6450501089238,336.373981573411));
#74126=CARTESIAN_POINT('Ctrl Pts',(76.994140341089,-1.89945010915349,340.490583336875));
#74127=CARTESIAN_POINT('Ctrl Pts',(76.7159023068151,3.5892472199492,339.568557812966));
#74128=CARTESIAN_POINT('Ctrl Pts',(76.4376642725411,5.78414535250674,334.454034215902));
#74129=CARTESIAN_POINT('Ctrl Pts',(76.1594262382672,2.6710186689145,329.840535360462));
#74130=CARTESIAN_POINT('Ctrl Pts',(75.8811882039932,-2.89326242296969,329.961801051152));
#74131=CARTESIAN_POINT('Ctrl Pts',(75.6029501697193,-5.80243929377797,334.706547553507));
#74132=CARTESIAN_POINT('Ctrl Pts',(75.3247121354454,-3.38680326854979,339.720591034656));
#74133=CARTESIAN_POINT('Ctrl Pts',(75.0464741011714,2.13685212709222,340.402617799111));
#74134=CARTESIAN_POINT('Ctrl Pts',(74.7682360668975,5.69954986558741,336.126741951831));
#74135=CARTESIAN_POINT('Ctrl Pts',(74.4899980326236,4.03185481765114,330.816871646039));
#74136=CARTESIAN_POINT('Ctrl Pts',(74.2117599983496,-1.33581388636402,329.345796487804));
#74137=CARTESIAN_POINT('Ctrl Pts',(73.9335219640757,-5.47762590344356,333.063500436805));
#74138=CARTESIAN_POINT('Ctrl Pts',(73.6552839298017,-4.59270147855875,338.558301452263));
#74139=CARTESIAN_POINT('Ctrl Pts',(73.3770458955278,0.506877305036717,340.787701745422));
#74140=CARTESIAN_POINT('Ctrl Pts',(73.0988078612539,5.14130226729675,337.705813573146));
#74141=CARTESIAN_POINT('Ctrl Pts',(72.8205698269799,5.05763002435563,332.140840222535));
#74142=CARTESIAN_POINT('Ctrl Pts',(72.542331792706,0.33264535856014,329.199675598576));
#74143=CARTESIAN_POINT('Ctrl Pts',(72.264093758432,-4.69760304294855,331.581383065154));
#74144=CARTESIAN_POINT('Ctrl Pts',(71.9858557241581,-5.41693046845061,337.100304834139));
#74145=CARTESIAN_POINT('Ctrl Pts',(71.7076176898843,-1.1652207568182,340.691807857282));
#74146=CARTESIAN_POINT('Ctrl Pts',(71.4293796556102,4.15579484471609,339.060022820744));
#74147=CARTESIAN_POINT('Ctrl Pts',(71.1511416213363,5.66309885668578,333.702414767449));
#74148=CARTESIAN_POINT('Ctrl Pts',(70.8729035870623,1.97346063507705,329.535581529739));
#74149=CARTESIAN_POINT('Ctrl Pts',(70.5946655527883,-3.52719328311067,330.383364467503));
#74150=CARTESIAN_POINT('Ctrl Pts',(70.3164275185145,-5.79099398667525,335.467765692012));
#74151=CARTESIAN_POINT('Ctrl Pts',(70.0381894842405,-2.74048498359907,340.122905245171));
#74152=CARTESIAN_POINT('Ctrl Pts',(69.7599514499667,2.8249266394339,340.076830268795));
#74153=CARTESIAN_POINT('Ctrl Pts',(69.4817134156927,5.79794478130726,335.371823088637));
#74154=CARTESIAN_POINT('Ctrl Pts',(69.2034753814187,3.45027457489966,330.325599348138));
#74155=CARTESIAN_POINT('Ctrl Pts',(68.9252373471448,-2.0636616829239,329.569004091811));
#74156=CARTESIAN_POINT('Ctrl Pts',(68.6469993128709,-5.68380607392486,333.796353619061));
#74157=CARTESIAN_POINT('Ctrl Pts',(68.3687612785969,-4.08800552372517,339.128271664307));
#74158=CARTESIAN_POINT('Ctrl Pts',(68.090523244323,1.25929735673448,340.671735736408));
#74159=CARTESIAN_POINT('Ctrl Pts',(67.8122852100489,5.45096164011743,337.01033163789));
#74160=CARTESIAN_POINT('Ctrl Pts',(67.5340471757753,4.64035888242653,331.504075867726));
#74161=CARTESIAN_POINT('Ctrl Pts',(67.255809141501,-0.428632730082352,329.205978073994));
#74162=CARTESIAN_POINT('Ctrl Pts',(66.9775711072273,-5.1042744128034,332.224968682135));
#74163=CARTESIAN_POINT('Ctrl Pts',(66.6993330729532,-5.09579880586159,337.790564571285));
#74164=CARTESIAN_POINT('Ctrl Pts',(66.4210950386793,-0.410983848647697,
340.795300542033));
#74165=CARTESIAN_POINT('Ctrl Pts',(66.1428570044054,4.65098492035853,338.481774743852));
#74166=CARTESIAN_POINT('Ctrl Pts',(65.8646189701315,5.44481347637662,332.97307565415));
#74167=CARTESIAN_POINT('Ctrl Pts',(65.5863809358575,1.24201707043907,329.324455119279));
#74168=CARTESIAN_POINT('Ctrl Pts',(65.3081429015836,-4.10056006889851,330.884198350542));
#74169=CARTESIAN_POINT('Ctrl Pts',(65.0299048673096,-5.68011375717534,336.220952006379));
#74170=CARTESIAN_POINT('Ctrl Pts',(64.7516668330357,-2.04711088883399,340.437256027184));
#74171=CARTESIAN_POINT('Ctrl Pts',(64.4734287987619,3.46449542688313,339.66387044561));
#74172=CARTESIAN_POINT('Ctrl Pts',(64.1951907644879,5.79678542521827,334.610519794715));
#74173=CARTESIAN_POINT('Ctrl Pts',(63.9169527302139,2.80945099924323,329.914589379491));
#74174=CARTESIAN_POINT('Ctrl Pts',(63.6387146959399,-2.75607514130854,329.885465230171));
#74175=CARTESIAN_POINT('Ctrl Pts',(63.360476661666,-5.79239180428386,334.549874148714));
#74176=CARTESIAN_POINT('Ctrl Pts',(63.0822386273922,-3.51311600403078,339.627356917135));
#74177=CARTESIAN_POINT('Ctrl Pts',(62.8040005931181,1.99009449961415,340.458382542378));
#74178=CARTESIAN_POINT('Ctrl Pts',(62.5257625588441,5.66702465470982,336.280331074075));
#74179=CARTESIAN_POINT('Ctrl Pts',(62.2475245245704,4.14340992932511,330.92733867675));
#74180=CARTESIAN_POINT('Ctrl Pts',(61.9692864902963,-1.18255093157096,329.311767463388));
#74181=CARTESIAN_POINT('Ctrl Pts',(61.6910484560225,-5.4233022569874,332.916203290701));
#74182=CARTESIAN_POINT('Ctrl Pts',(61.4128104217484,-4.68716914897679,338.432908601349));
#74183=CARTESIAN_POINT('Ctrl Pts',(61.1345723874745,0.350309904546443,340.799284358187));
#74184=CARTESIAN_POINT('Ctrl Pts',(60.8563343532007,5.06631472923324,337.843742456814));
#74185=CARTESIAN_POINT('Ctrl Pts',(60.5780963189266,5.1330373055855,332.278540076393));
#74186=CARTESIAN_POINT('Ctrl Pts',(60.2998582846528,0.489247310108402,329.210781299184));
#74187=CARTESIAN_POINT('Ctrl Pts',(60.0216202503787,-4.60351772057673,331.455703074986));
#74188=CARTESIAN_POINT('Ctrl Pts',(59.743382216105,-5.47170248689875,336.953173825136));
#74189=CARTESIAN_POINT('Ctrl Pts',(59.4651441818308,-1.31858664319012,340.658245784758));
#74190=CARTESIAN_POINT('Ctrl Pts',(59.186906147557,4.04457670066713,339.170829103278));
#74191=CARTESIAN_POINT('Ctrl Pts',(58.9086681132829,5.69609170417641,333.855904115056));
#74192=CARTESIAN_POINT('Ctrl Pts',(58.6304300790092,2.12038742493874,329.59089903362));
#74193=CARTESIAN_POINT('Ctrl Pts',(58.3521920447351,-3.40116509729812,330.289746070831));
#74194=CARTESIAN_POINT('Ctrl Pts',(58.0739540104613,-5.80151861085904,335.311123615607));
#74195=CARTESIAN_POINT('Ctrl Pts',(57.7957159761872,-2.87790412550895,340.046987610516));
#74196=CARTESIAN_POINT('Ctrl Pts',(57.5174779419134,2.68672049802545,340.151305568671));
#74197=CARTESIAN_POINT('Ctrl Pts',(57.2392399076394,5.78578137645143,335.528346439601));
#74198=CARTESIAN_POINT('Ctrl Pts',(56.9610018733654,3.57531608370108,330.42053158129));
#74199=CARTESIAN_POINT('Ctrl Pts',(56.6827638390915,-1.91616400748287,329.515227297986));
#74200=CARTESIAN_POINT('Ctrl Pts',(56.4045258048175,-5.64920867153418,333.643217968208));
#74201=CARTESIAN_POINT('Ctrl Pts',(56.1262877705437,-4.19805791990187,339.016307482935));
#74202=CARTESIAN_POINT('Ctrl Pts',(55.8480497362697,1.10558862159104,340.703690901174));
#74203=CARTESIAN_POINT('Ctrl Pts',(55.5698117019958,5.39465280351117,337.156881365746));
#74204=CARTESIAN_POINT('Ctrl Pts',(55.2915736677218,4.73312373259396,331.630733636489));
#74205=CARTESIAN_POINT('Ctrl Pts',(55.013335633448,-0.271923126932959,329.196511918736));
#74206=CARTESIAN_POINT('Ctrl Pts',(54.7350975991739,-5.02743014645227,332.088065553816));
#74207=CARTESIAN_POINT('Ctrl Pts',(54.4568595649,-5.16933872531966,337.651858450077));
#74208=CARTESIAN_POINT('Ctrl Pts',(54.1786215306261,-0.567421455275803,
340.782079988069));
#74209=CARTESIAN_POINT('Ctrl Pts',(53.9003834963521,4.55521010914761,338.606172064372));
#74210=CARTESIAN_POINT('Ctrl Pts',(53.6221454620782,5.49759259119749,333.120933264213));
#74211=CARTESIAN_POINT('Ctrl Pts',(53.3439074278042,1.39491549663908,329.360086272507));
#74212=CARTESIAN_POINT('Ctrl Pts',(53.0656693935303,-3.98785496026603,330.774904863531));
#74213=CARTESIAN_POINT('Ctrl Pts',(52.7874313592564,-5.71102978077773,336.067030898991));
#74214=CARTESIAN_POINT('Ctrl Pts',(52.5091933249824,-2.1932768661311,340.379958427797));
#74215=CARTESIAN_POINT('Ctrl Pts',(52.2309552907086,3.33721385585057,339.75577751547));
#74216=CARTESIAN_POINT('Ctrl Pts',(51.9527172564345,5.80519267951394,334.767289772358));
#74217=CARTESIAN_POINT('Ctrl Pts',(51.6744792221607,2.94583186569086,329.992356770355));
#74218=CARTESIAN_POINT('Ctrl Pts',(51.3962411878866,-2.61687537086965,329.812864047505));
#74219=CARTESIAN_POINT('Ctrl Pts',(51.1180031536129,-5.77811470460025,334.393529426259));
#74220=CARTESIAN_POINT('Ctrl Pts',(50.8397651193388,-3.63686345875244,339.530743899044));
#74221=CARTESIAN_POINT('Ctrl Pts',(50.561527085065,1.84188370317583,340.510161569346));
#74222=CARTESIAN_POINT('Ctrl Pts',(50.283289050791,5.63036137685853,336.432985297313));
#74223=CARTESIAN_POINT('Ctrl Pts',(50.005051016517,4.25193951899586,331.040779568762));
#74224=CARTESIAN_POINT('Ctrl Pts',(49.726812982243,-1.02842447692488,329.281891991962));
#74225=CARTESIAN_POINT('Ctrl Pts',(49.4485749479692,-5.36501850989206,332.770427735001));
#74226=CARTESIAN_POINT('Ctrl Pts',(49.1703369136951,-4.77821424387469,338.305009037199));
#74227=CARTESIAN_POINT('Ctrl Pts',(48.8920988794214,0.193486707419849,340.806632327811));
#74228=CARTESIAN_POINT('Ctrl Pts',(48.6138608451472,4.98762776317431,337.979594836945));
#74229=CARTESIAN_POINT('Ctrl Pts',(48.3356228108734,5.20469643792882,332.418227142961));
#74230=CARTESIAN_POINT('Ctrl Pts',(48.0573847765994,0.645492012789552,329.226114292978));
#74231=CARTESIAN_POINT('Ctrl Pts',(47.7791467423257,-4.50607090504021,331.332611133916));
#74232=CARTESIAN_POINT('Ctrl Pts',(47.5009087080515,-5.52247906281209,336.804616606687));
#74233=CARTESIAN_POINT('Ctrl Pts',(47.2226706737776,-1.47098969629869,340.620552055601));
#74234=CARTESIAN_POINT('Ctrl Pts',(46.9444326395036,3.93040520273572,339.2785898423));
#74235=CARTESIAN_POINT('Ctrl Pts',(46.6661946052298,5.72492525990519,334.010228882605));
#74236=CARTESIAN_POINT('Ctrl Pts',(46.3879565709557,2.26576590581826,329.650166268343));
#74237=CARTESIAN_POINT('Ctrl Pts',(46.1097185366819,-3.27265337738824,330.199567106209));
#74238=CARTESIAN_POINT('Ctrl Pts',(45.8314805024079,-5.80780696045024,335.154254356432));
#74239=CARTESIAN_POINT('Ctrl Pts',(45.5532424681341,-3.01322181899706,339.967384660549));
#74240=CARTESIAN_POINT('Ctrl Pts',(45.27500443386,2.54655251066853,340.222019380158));
#74241=CARTESIAN_POINT('Ctrl Pts',(44.9967663995862,5.76939318834706,335.684483991476));
#74242=CARTESIAN_POINT('Ctrl Pts',(44.7185283653121,3.69774689318336,330.518807746783));
#74243=CARTESIAN_POINT('Ctrl Pts',(44.4402903310382,-1.76726714720003,329.46545549058));
#74244=CARTESIAN_POINT('Ctrl Pts',(44.1620522967642,-5.61048621141828,333.491073040927));
#74245=CARTESIAN_POINT('Ctrl Pts',(43.8838142624904,-4.30504489005872,338.901410589891));
#74246=CARTESIAN_POINT('Ctrl Pts',(43.6055762282163,0.951072584549313,340.731481225237));
#74247=CARTESIAN_POINT('Ctrl Pts',(43.3273381939426,5.33440478612478,337.301856136709));
#74248=CARTESIAN_POINT('Ctrl Pts',(43.0491001596685,4.82243245115911,331.759851646862));
#74249=CARTESIAN_POINT('Ctrl Pts',(42.7708621253947,-0.115014965248771,
329.191283476181));
#74250=CARTESIAN_POINT('Ctrl Pts',(42.4926240911207,-4.94691484566584,331.95328872289));
#74251=CARTESIAN_POINT('Ctrl Pts',(42.2143860568467,-5.23910398855925,337.511215939221));
#74252=CARTESIAN_POINT('Ctrl Pts',(41.9361480225728,-0.723444730199963,
340.764637353613));
#74253=CARTESIAN_POINT('Ctrl Pts',(41.6579099882988,4.45610907903712,338.727936154504));
#74254=CARTESIAN_POINT('Ctrl Pts',(41.379671954025,5.54635735850404,333.270162970653));
#74255=CARTESIAN_POINT('Ctrl Pts',(41.1014339197509,1.5467953541722,329.399835696282));
#74256=CARTESIAN_POINT('Ctrl Pts',(40.8231958854771,-3.87223791602144,330.668696545143));
#74257=CARTESIAN_POINT('Ctrl Pts',(40.5449578512032,-5.73777560482017,335.912330644593));
#74258=CARTESIAN_POINT('Ctrl Pts',(40.2667198169292,-2.33784131050453,340.318732377478));
#74259=CARTESIAN_POINT('Ctrl Pts',(39.9884817826552,3.20749544797993,339.844211911913));
#74260=CARTESIAN_POINT('Ctrl Pts',(39.7102437483813,5.80936097640842,334.924229675237));
#74261=CARTESIAN_POINT('Ctrl Pts',(39.4320057141073,3.08006168281437,330.073780747227));
#74262=CARTESIAN_POINT('Ctrl Pts',(39.1537676798335,-2.47576475546252,329.74405051661));
#74263=CARTESIAN_POINT('Ctrl Pts',(38.8755296455594,-5.75961841987933,334.237627549214));
#74264=CARTESIAN_POINT('Ctrl Pts',(38.5972916112856,-3.75795527220141,339.430822527304));
#74265=CARTESIAN_POINT('Ctrl Pts',(38.3190535770116,1.69232796144685,340.557917070921));
#74266=CARTESIAN_POINT('Ctrl Pts',(38.0408155427377,5.58958680359511,336.584593153275));
#74267=CARTESIAN_POINT('Ctrl Pts',(37.7625775084637,4.35736433825011,331.157111487425));
#74268=CARTESIAN_POINT('Ctrl Pts',(37.4843394741898,-0.873547065714799,
329.256191888624));
#74269=CARTESIAN_POINT('Ctrl Pts',(37.2061014399158,-5.3028172210068,332.626280215163));
#74270=CARTESIAN_POINT('Ctrl Pts',(36.9278634056419,-4.86577028203474,338.174696152201));
#74271=CARTESIAN_POINT('Ctrl Pts',(36.649625371368,0.0365222261089616,340.809740288802));
#74272=CARTESIAN_POINT('Ctrl Pts',(36.3713873370941,4.90529882641964,338.113271513996));
#74273=CARTESIAN_POINT('Ctrl Pts',(36.0931493028201,5.27255509581702,332.559799422608));
#74274=CARTESIAN_POINT('Ctrl Pts',(35.8149112685462,0.801265376568756,329.245663383792));
#74275=CARTESIAN_POINT('Ctrl Pts',(35.5366732342722,-4.40533375209907,331.2121971238));
#74276=CARTESIAN_POINT('Ctrl Pts',(35.2584351999983,-5.56922311908519,336.654741655419));
#74277=CARTESIAN_POINT('Ctrl Pts',(34.9801971657244,-1.62231863128531,340.578754193806));
#74278=CARTESIAN_POINT('Ctrl Pts',(34.7019591314504,3.81336371906134,339.383226350815));
#74279=CARTESIAN_POINT('Ctrl Pts',(34.4237210971765,5.74957846958163,334.165276381994));
#74280=CARTESIAN_POINT('Ctrl Pts',(34.1454830629025,2.40948992220596,329.713339956918));
#74281=CARTESIAN_POINT('Ctrl Pts',(33.8672450286286,-3.14175196276516,330.112893422403));
#74282=CARTESIAN_POINT('Ctrl Pts',(33.5890069943546,-5.80985444368967,334.997272460574));
#74283=CARTESIAN_POINT('Ctrl Pts',(33.3107689600807,-3.14633925495117,339.884154521417));
#74284=CARTESIAN_POINT('Ctrl Pts',(33.0325309258068,2.40452502816473,340.28892006796));
#74285=CARTESIAN_POINT('Ctrl Pts',(32.7542928915328,5.74879218366509,335.840121732466));
#74286=CARTESIAN_POINT('Ctrl Pts',(32.4760548572589,3.81747760424955,330.620356083268));
#74287=CARTESIAN_POINT('Ctrl Pts',(32.1978168229849,-1.61707982670873,329.419725013012));
#74288=CARTESIAN_POINT('Ctrl Pts',(31.919578788711,-5.56766696875553,333.340029933596));
#74289=CARTESIAN_POINT('Ctrl Pts',(31.6413407544371,-4.40888831220513,338.783664882997));
#74290=CARTESIAN_POINT('Ctrl Pts',(31.3631027201632,0.795862073371101,340.755086416076));
#74291=CARTESIAN_POINT('Ctrl Pts',(31.0848646858892,5.27026158111962,337.445150090057));
#74292=CARTESIAN_POINT('Ctrl Pts',(30.8066266516153,4.90821982480809,331.89133561675));
#74293=CARTESIAN_POINT('Ctrl Pts',(30.5283886173413,0.0419771804760357,
329.190296564138));
#74294=CARTESIAN_POINT('Ctrl Pts',(30.2501505830674,-4.8627873027967,331.820736603537));
#74295=CARTESIAN_POINT('Ctrl Pts',(29.9719125487934,-5.30504365291584,337.368739736017));
#74296=CARTESIAN_POINT('Ctrl Pts',(29.6936745145195,-0.87893974507008,340.742985375297));
#74297=CARTESIAN_POINT('Ctrl Pts',(29.4154364802456,4.35375419369712,338.84697810199));
#74298=CARTESIAN_POINT('Ctrl Pts',(29.1371984459716,5.59107217021504,333.420655805792));
#74299=CARTESIAN_POINT('Ctrl Pts',(28.8589604116977,1.69754574021657,329.443674365535));
#74300=CARTESIAN_POINT('Ctrl Pts',(28.5807223774237,-3.75379335984459,330.565650948796));
#74301=CARTESIAN_POINT('Ctrl Pts',(28.3024843431498,-5.76033169947554,335.75696420546));
#74302=CARTESIAN_POINT('Ctrl Pts',(28.0242463088759,-2.48069866085444,340.253622583549));
#74303=CARTESIAN_POINT('Ctrl Pts',(27.746008274602,3.07543492378025,339.929109060055));
#74304=CARTESIAN_POINT('Ctrl Pts',(27.467770240328,5.80928727220723,335.081224905682));
#74305=CARTESIAN_POINT('Ctrl Pts',(27.1895322060541,3.21204243586931,330.15880185424));
#74306=CARTESIAN_POINT('Ctrl Pts',(26.9112941717801,-2.33284633419722,329.679074885196));
#74307=CARTESIAN_POINT('Ctrl Pts',(26.6330561375062,-5.73691645612644,334.082282357281));
#74308=CARTESIAN_POINT('Ctrl Pts',(26.3548181032323,-3.87630302301649,339.3276657646));
#74309=CARTESIAN_POINT('Ctrl Pts',(26.0765800689583,1.54153648017683,340.601614175988));
#74310=CARTESIAN_POINT('Ctrl Pts',(25.7983420346844,5.54473070855304,336.73504393776));
#74311=CARTESIAN_POINT('Ctrl Pts',(25.5201040004104,4.45960740578122,331.276249487059));
#74312=CARTESIAN_POINT('Ctrl Pts',(25.2418659661365,-0.718031789578611,
329.234685919615));
#74313=CARTESIAN_POINT('Ctrl Pts',(24.9636279318626,-5.236743809774,332.483865987845));
#74314=CARTESIAN_POINT('Ctrl Pts',(24.6853898975886,-4.9497733299517,338.042065100952));
#74315=CARTESIAN_POINT('Ctrl Pts',(24.4071518633147,-0.120468923767338,
340.808605971724));
#74316=CARTESIAN_POINT('Ctrl Pts',(24.1289138290407,4.81938803563992,338.244674877127));
#74317=CARTESIAN_POINT('Ctrl Pts',(23.8506757947668,5.33656372879123,332.703153539115));
#74318=CARTESIAN_POINT('Ctrl Pts',(23.5724377604928,0.956453655582346,329.269414296857));
#74319=CARTESIAN_POINT('Ctrl Pts',(23.294199726219,-4.30137982012164,331.094548971069));
#74320=CARTESIAN_POINT('Ctrl Pts',(23.0159616919449,-5.61190052316207,336.503658410166));
#74321=CARTESIAN_POINT('Ctrl Pts',(22.7377236576712,-1.77246294761261,340.532882720216));
#74322=CARTESIAN_POINT('Ctrl Pts',(22.4594856233971,3.69353771345072,339.484662223139));
#74323=CARTESIAN_POINT('Ctrl Pts',(22.1812475891232,5.77003333140761,334.320933397392));
#74324=CARTESIAN_POINT('Ctrl Pts',(21.9030095548492,2.55145452668411,329.780373969853));
#74325=CARTESIAN_POINT('Ctrl Pts',(21.6247715205754,-3.00855643777032,330.029788308625));
#74326=CARTESIAN_POINT('Ctrl Pts',(21.3465334863014,-5.80765956550315,334.840292556368));
#74327=CARTESIAN_POINT('Ctrl Pts',(21.0682954520274,-3.27715923088842,339.797357967855));
#74328=CARTESIAN_POINT('Ctrl Pts',(20.7900574177535,2.26074175912166,340.351958781128));
#74329=CARTESIAN_POINT('Ctrl Pts',(20.5118193834796,5.72399340527947,335.995146015743));
#74330=CARTESIAN_POINT('Ctrl Pts',(20.2335813492056,3.93442078941648,330.725102440042));
#74331=CARTESIAN_POINT('Ctrl Pts',(19.9553433149317,-1.46571171293835,329.37806925773));
#74332=CARTESIAN_POINT('Ctrl Pts',(19.6771052806577,-5.52078221019907,333.190198938037));
#74333=CARTESIAN_POINT('Ctrl Pts',(19.3988672463838,-4.50951235977196,338.663156340289));
#74334=CARTESIAN_POINT('Ctrl Pts',(19.1206292121098,0.640070422924563,340.774489237156));
#74335=CARTESIAN_POINT('Ctrl Pts',(18.842391177836,5.20227002592717,337.586658592407));
#74336=CARTESIAN_POINT('Ctrl Pts',(18.5641531435619,4.99042321151613,332.025089536424));
#74337=CARTESIAN_POINT('Ctrl Pts',(18.2859151092881,0.198938674422592,329.193551903259));
#74338=CARTESIAN_POINT('Ctrl Pts',(18.0076770750141,-4.77510894785852,331.690505985439));
#74339=CARTESIAN_POINT('Ctrl Pts',(17.7294390407402,-5.36710956918242,337.224533876731));
#74340=CARTESIAN_POINT('Ctrl Pts',(17.4512010064662,-1.03379295727499,340.717139863413));
#74341=CARTESIAN_POINT('Ctrl Pts',(17.1729629721923,4.24822019276465,338.963210982287));
#74342=CARTESIAN_POINT('Ctrl Pts',(16.8947249379183,5.63170437553145,333.572301879615));
#74343=CARTESIAN_POINT('Ctrl Pts',(16.6164869036444,1.84705657669332,329.49157026923));
#74344=CARTESIAN_POINT('Ctrl Pts',(16.3382488693705,-3.63260778006579,330.465843318484));
#74345=CARTESIAN_POINT('Ctrl Pts',(16.0600108350965,-5.77868159426167,335.601045030322));
#74346=CARTESIAN_POINT('Ctrl Pts',(15.7817728008226,-2.62174460260375,340.184676589243));
#74347=CARTESIAN_POINT('Ctrl Pts',(15.5035347665486,2.94112871397601,340.010406967918));
#74348=CARTESIAN_POINT('Ctrl Pts',(15.2252967322747,5.80497162072999,335.238160825619));
#74349=CARTESIAN_POINT('Ctrl Pts',(14.9470586980008,3.34167775237819,330.247358008898));
#74350=CARTESIAN_POINT('Ctrl Pts',(14.6688206637269,-2.18822446624349,329.617984598531));
#74351=CARTESIAN_POINT('Ctrl Pts',(14.3905826294529,-5.71002539034279,333.927607283674));
#74352=CARTESIAN_POINT('Ctrl Pts',(14.1123445951789,-3.99182029354395,339.221348936101));
#74353=CARTESIAN_POINT('Ctrl Pts',(13.834106560905,1.38961936743681,340.641220976873));
#74354=CARTESIAN_POINT('Ctrl Pts',(13.5558685266311,5.49582584573023,336.884227791461));
#74355=CARTESIAN_POINT('Ctrl Pts',(13.2776304923572,4.55859406353803,331.398106572968));
#74356=CARTESIAN_POINT('Ctrl Pts',(12.9993924580832,-0.561992205806647,
329.217389788631));
#74357=CARTESIAN_POINT('Ctrl Pts',(12.7211544238093,-5.16684652328562,332.343289044026));
#74358=CARTESIAN_POINT('Ctrl Pts',(12.4429163895354,-5.03016204809799,337.90721273083));
#74359=CARTESIAN_POINT('Ctrl Pts',(12.1646783552614,-0.277372107909085,
340.803230204752));
#74360=CARTESIAN_POINT('Ctrl Pts',(11.8864403209875,4.72995812447452,338.373708975665));
#74361=CARTESIAN_POINT('Ctrl Pts',(11.6082022867135,5.39667559486097,332.848184814806));
#74362=CARTESIAN_POINT('Ctrl Pts',(11.3299642524396,1.11094353652828,329.297349689919));
#74363=CARTESIAN_POINT('Ctrl Pts',(11.0517262181657,-4.19428502643889,330.979752581234));
#74364=CARTESIAN_POINT('Ctrl Pts',(10.7734881838918,-5.65048009295057,336.351477194488));
#74365=CARTESIAN_POINT('Ctrl Pts',(10.4952501496178,-1.92131304564754,340.482971125652));
#74366=CARTESIAN_POINT('Ctrl Pts',(10.2170121153439,3.57101475074672,339.582823399336));
#74367=CARTESIAN_POINT('Ctrl Pts',(9.93877408106996,5.78627478124848,334.477086251583));
#74368=CARTESIAN_POINT('Ctrl Pts',(9.66053604679602,2.69155629820058,329.851219389636));
#74369=CARTESIAN_POINT('Ctrl Pts',(9.38229801252208,-2.87316451817608,329.95031239017));
#74370=CARTESIAN_POINT('Ctrl Pts',(9.10405997824813,-5.80122306706437,334.683429380474));
#74371=CARTESIAN_POINT('Ctrl Pts',(8.82582194397421,-3.40558784867484,339.707058171501));
#74372=CARTESIAN_POINT('Ctrl Pts',(8.54758390970025,2.11531076584172,340.41108988013));
#74373=CARTESIAN_POINT('Ctrl Pts',(8.26934587542634,5.69500916144305,336.149442903385));
#74374=CARTESIAN_POINT('Ctrl Pts',(7.9911078411524,4.04850200793196,330.832971726666));
#74375=CARTESIAN_POINT('Ctrl Pts',(7.71286980687842,-1.31329401327319,329.340516006911));
#74376=CARTESIAN_POINT('Ctrl Pts',(7.43463177260454,-5.46982712631381,333.041694436197));
#74377=CARTESIAN_POINT('Ctrl Pts',(7.15639373833055,-4.60691728147025,338.539963563042));
#74378=CARTESIAN_POINT('Ctrl Pts',(6.87815570405667,0.483950600032991,340.789693258488));
#74379=CARTESIAN_POINT('Ctrl Pts',(6.59991766978268,5.13021690941976,337.726244822412));
#74380=CARTESIAN_POINT('Ctrl Pts',(6.32167963550878,5.06947896879733,332.161078968005));
#74381=CARTESIAN_POINT('Ctrl Pts',(6.0434416012348,0.354817207204381,329.200927806512));
#74382=CARTESIAN_POINT('Ctrl Pts',(5.7652035669609,-4.68216976966421,331.56291659117));
#74383=CARTESIAN_POINT('Ctrl Pts',(5.48696553268694,-5.42863455194625,337.078284863033));
#74384=CARTESIAN_POINT('Ctrl Pts',(5.208727498413,-1.18128049517348,340.687866433408));
#74385=CARTESIAN_POINT('Ctrl Pts',(4.9768624698514,3.24078857374305,339.344254515386));
#74386=CARTESIAN_POINT('Ctrl Pts',(4.79137044700209,4.91809615913057,336.398020145725));
#74387=CARTESIAN_POINT('Ctrl Pts',(4.69862443557744,4.97290566312669,334.719862138));
#74388=CARTESIAN_POINT('Ctrl Pts',(4.65225142986512,4.79338446579369,333.921776804495));
#74389=CARTESIAN_POINT('Ctrl Pts',(5.23167681249901,-1.34668115311846,339.737346666877));
#74390=CARTESIAN_POINT('Ctrl Pts',(5.23167681249889,-1.23675483698737,339.781456312384));
#74391=CARTESIAN_POINT('Ctrl Pts',(5.23167681249914,-1.12542425527317,339.821231768089));
#74392=CARTESIAN_POINT('Ctrl Pts',(5.2316768124991,-1.01288792298132,339.85652298731));
#74393=CARTESIAN_POINT('Ctrl Pts',(5.23167681249901,-0.877572330351241,
339.898957747234));
#74394=CARTESIAN_POINT('Ctrl Pts',(5.23167681249896,-0.740514058238084,
339.934911453407));
#74395=CARTESIAN_POINT('Ctrl Pts',(5.23167681249902,-0.602118655133099,
339.96460111858));
#74396=CARTESIAN_POINT('Ctrl Pts',(5.23167681249908,-0.463723252028115,
339.994290783752));
#74397=CARTESIAN_POINT('Ctrl Pts',(5.23167681249919,-0.323990096019264,
340.017716363323));
#74398=CARTESIAN_POINT('Ctrl Pts',(5.23167681249908,-0.183299247619329,
340.035048214569));
#74399=CARTESIAN_POINT('Ctrl Pts',(5.23167681249896,-0.0386841920429301,
340.05286349296));
#74400=CARTESIAN_POINT('Ctrl Pts',(5.23167681249883,0.106943343603134,340.06424054752));
#74401=CARTESIAN_POINT('Ctrl Pts',(5.23167681249904,0.253188220578269,340.069313737644));
#74402=CARTESIAN_POINT('Ctrl Pts',(5.23167681249916,0.334525544479147,340.072135304572));
#74403=CARTESIAN_POINT('Ctrl Pts',(5.23167681249893,0.416054086959694,340.073006003226));
#74404=CARTESIAN_POINT('Ctrl Pts',(5.23167681249885,0.49770699289044,340.071942155002));
#74405=CARTESIAN_POINT('Ctrl Pts',(5.23167681249882,0.526903163358536,340.071561760774));
#74406=CARTESIAN_POINT('Ctrl Pts',(5.23167681249909,0.556122147452936,340.070933686722));
#74407=CARTESIAN_POINT('Ctrl Pts',(5.23167681249904,0.585323801418764,340.070059915179));
#74408=CARTESIAN_POINT('Ctrl Pts',(5.23167681249883,0.734801547718469,340.06558724383));
#74409=CARTESIAN_POINT('Ctrl Pts',(5.23167681249919,0.883962607076913,340.0546820683));
#74410=CARTESIAN_POINT('Ctrl Pts',(5.23167681249915,1.0323778451602,340.037563106176));
#74411=CARTESIAN_POINT('Ctrl Pts',(5.23167681249911,1.18269721686223,340.020224511677));
#74412=CARTESIAN_POINT('Ctrl Pts',(5.23167681249882,1.33225222875417,339.996511689538));
#74413=CARTESIAN_POINT('Ctrl Pts',(5.23167681249888,1.48061471242626,339.966599919862));
#74414=CARTESIAN_POINT('Ctrl Pts',(5.23167681249894,1.63042017296366,339.936397227639));
#74415=CARTESIAN_POINT('Ctrl Pts',(5.2316768124989,1.77901059605625,339.899874418231));
#74416=CARTESIAN_POINT('Ctrl Pts',(5.23167681249895,1.9259515555415,339.857159153423));
#74417=CARTESIAN_POINT('Ctrl Pts',(5.231676812499,2.07258551961732,339.814533131194));
#74418=CARTESIAN_POINT('Ctrl Pts',(5.23167681249901,2.21757773979494,339.765740402025));
#74419=CARTESIAN_POINT('Ctrl Pts',(5.23167681249909,2.36049050053187,339.710856434616));
#74420=CARTESIAN_POINT('Ctrl Pts',(5.23167681249913,2.40223249230077,339.694825912891));
#74421=CARTESIAN_POINT('Ctrl Pts',(5.23167681249891,2.44379699939896,339.678275412879));
#74422=CARTESIAN_POINT('Ctrl Pts',(5.23167681249902,2.48517285780773,339.661206003771));
#74423=CARTESIAN_POINT('Ctrl Pts',(5.23167681249904,2.50433078795608,339.653302492885));
#74424=CARTESIAN_POINT('Ctrl Pts',(5.23167681249916,2.52344916383466,339.645287290512));
#74425=CARTESIAN_POINT('Ctrl Pts',(5.23167681249915,2.54251135007745,339.637167259143));
#74426=CARTESIAN_POINT('Ctrl Pts',(5.2316768124989,2.68705304330757,339.575595985614));
#74427=CARTESIAN_POINT('Ctrl Pts',(5.23167681249902,2.82857221596661,339.50791689713));
#74428=CARTESIAN_POINT('Ctrl Pts',(5.23167681249907,2.96662330249087,339.434312734319));
#74429=CARTESIAN_POINT('Ctrl Pts',(5.23167681249911,3.10460481213973,339.360745667541));
#74430=CARTESIAN_POINT('Ctrl Pts',(5.23167681249916,3.23912257405703,339.281259374025));
#74431=CARTESIAN_POINT('Ctrl Pts',(5.23167681249917,3.36972909595313,339.195984735696));
#74432=CARTESIAN_POINT('Ctrl Pts',(5.23167681249917,3.49947681772413,339.111270818753));
#74433=CARTESIAN_POINT('Ctrl Pts',(5.23167681249904,3.62536538725959,339.02084426393));
#74434=CARTESIAN_POINT('Ctrl Pts',(5.23167681249888,3.74694111839647,338.924784699129));
#74435=CARTESIAN_POINT('Ctrl Pts',(5.23167681249882,3.79095071680503,338.890011781618));
#74436=CARTESIAN_POINT('Ctrl Pts',(5.23167681249915,3.83439496160363,338.854500266954));
#74437=CARTESIAN_POINT('Ctrl Pts',(5.23167681249907,3.87725152194784,338.818252407266));
#74438=CARTESIAN_POINT('Ctrl Pts',(5.23167681249883,3.98972601993342,338.723122051758));
#74439=CARTESIAN_POINT('Ctrl Pts',(5.23167681249901,4.09815478095222,338.622922413815));
#74440=CARTESIAN_POINT('Ctrl Pts',(5.2316768124991,4.20239332039485,338.518019138625));
#74441=CARTESIAN_POINT('Ctrl Pts',(5.23167681249906,4.22019037122658,338.500108594876));
#74442=CARTESIAN_POINT('Ctrl Pts',(5.23167681249891,4.23786747898358,338.482058400429));
#74443=CARTESIAN_POINT('Ctrl Pts',(5.23167681249894,4.2554061724232,338.463888906878));
#74444=CARTESIAN_POINT('Ctrl Pts',(5.23167681249913,4.36250722519882,338.352935836487));
#74445=CARTESIAN_POINT('Ctrl Pts',(5.23167681249885,4.46458172457174,338.237406884179));
#74446=CARTESIAN_POINT('Ctrl Pts',(5.23167681249892,4.56153344475904,338.117806877089));
#74447=CARTESIAN_POINT('Ctrl Pts',(5.23167681249899,4.66017670753057,337.996120176697));
#74448=CARTESIAN_POINT('Ctrl Pts',(5.23167681249898,4.75351731967113,337.870218648565));
#74449=CARTESIAN_POINT('Ctrl Pts',(5.23167681249897,4.8414280052284,337.740585136994));
#74450=CARTESIAN_POINT('Ctrl Pts',(5.23167681249896,4.93094693812344,337.608580096313));
#74451=CARTESIAN_POINT('Ctrl Pts',(5.23167681249902,5.01483597188807,337.472704727081));
#74452=CARTESIAN_POINT('Ctrl Pts',(5.23167681249905,5.09292670865521,337.333426458399));
#74453=CARTESIAN_POINT('Ctrl Pts',(5.23167681249908,5.16249416850671,337.209349829519));
#74454=CARTESIAN_POINT('Ctrl Pts',(5.23167681249896,5.22745971835016,337.082571668943));
#74455=CARTESIAN_POINT('Ctrl Pts',(5.231676812499,5.28767719560329,336.953400592671));
#74456=CARTESIAN_POINT('Ctrl Pts',(5.231676812499,5.31803717586098,336.888276122096));
#74457=CARTESIAN_POINT('Ctrl Pts',(5.23167681249893,5.34718981662582,336.822543112078));
#74458=CARTESIAN_POINT('Ctrl Pts',(5.23167681249895,5.37511360302354,336.756239639658));
#74459=CARTESIAN_POINT('Ctrl Pts',(5.23167681249897,5.38387786312344,336.735429393169));
#74460=CARTESIAN_POINT('Ctrl Pts',(5.23167681249899,5.3925210537521,336.714562944136));
#74461=CARTESIAN_POINT('Ctrl Pts',(5.23167681249894,5.40104246900692,336.693641454162));
#74462=CARTESIAN_POINT('Ctrl Pts',(5.23167681249891,5.40897664218581,336.674161741032));
#74463=CARTESIAN_POINT('Ctrl Pts',(5.231676812499,5.41680164871212,336.654643136502));
#74464=CARTESIAN_POINT('Ctrl Pts',(5.23167681249898,5.42451698628412,336.635087237854));
#74465=CARTESIAN_POINT('Ctrl Pts',(5.23167681249897,5.43491648844008,336.608727845506));
#74466=CARTESIAN_POINT('Ctrl Pts',(5.23167681249902,5.44511686297811,336.582300399227));
#74467=CARTESIAN_POINT('Ctrl Pts',(5.23167681249901,5.45511734450837,336.555807568461));
#74468=CARTESIAN_POINT('Ctrl Pts',(5.23167681249897,5.51276118082839,336.403100081758));
#74469=CARTESIAN_POINT('Ctrl Pts',(5.231676812499,5.56376708959899,336.248222805456));
#74470=CARTESIAN_POINT('Ctrl Pts',(5.23167681249898,5.60813990494374,336.091593888462));
#74471=CARTESIAN_POINT('Ctrl Pts',(5.23167681249896,5.65251272028848,335.934964971469));
#74472=CARTESIAN_POINT('Ctrl Pts',(5.23167681249898,5.69025265554719,335.776583766993));
#74473=CARTESIAN_POINT('Ctrl Pts',(5.231676812499,5.72131952430206,335.616841802708));
#74474=CARTESIAN_POINT('Ctrl Pts',(5.23167681249901,5.73662548264904,335.538140473941));
#74475=CARTESIAN_POINT('Ctrl Pts',(5.23167681249891,5.75031096821763,335.459108498761));
#74476=CARTESIAN_POINT('Ctrl Pts',(5.23167681249892,5.76236691005121,335.379791061143));
#74477=CARTESIAN_POINT('Ctrl Pts',(5.23167681249892,5.76818605760889,335.341506215399));
#74478=CARTESIAN_POINT('Ctrl Pts',(5.23167681249898,5.77362551299829,335.303154849943));
#74479=CARTESIAN_POINT('Ctrl Pts',(5.23167681249898,5.77868401197528,335.264741983279));
#74480=CARTESIAN_POINT('Ctrl Pts',(5.231676812499,5.78204651990671,335.239208011756));
#74481=CARTESIAN_POINT('Ctrl Pts',(5.23167681249895,5.78524069104185,335.213646366837));
#74482=CARTESIAN_POINT('Ctrl Pts',(5.23167681249898,5.78826445021777,335.188074200246));
#74483=CARTESIAN_POINT('Ctrl Pts',(5.231676812499,5.80778662166987,335.022973677496));
#74484=CARTESIAN_POINT('Ctrl Pts',(5.231676812499,5.82023072297851,334.857279926282));
#74485=CARTESIAN_POINT('Ctrl Pts',(5.231676812499,5.82557797797662,334.691409186639));
#74486=CARTESIAN_POINT('Ctrl Pts',(5.23167681249897,5.83090854965785,334.526055960018));
#74487=CARTESIAN_POINT('Ctrl Pts',(5.23167681249901,5.82918667389409,334.360526158613));
#74488=CARTESIAN_POINT('Ctrl Pts',(5.23167681249899,5.82034517345234,334.195215344822));
#74489=CARTESIAN_POINT('Ctrl Pts',(5.23167681249896,5.81152526086727,334.030308162313));
#74490=CARTESIAN_POINT('Ctrl Pts',(5.23167681249899,5.79562064591606,333.865618214986));
#74491=CARTESIAN_POINT('Ctrl Pts',(5.23167681249902,5.77251337094751,333.701531692827));
#74492=CARTESIAN_POINT('Origin',(5.23167681249902,0.,335.));
#74511=UNCERTAINTY_MEASURE_WITH_UNIT(LENGTH_MEASURE(0.01),#74524,
'DISTANCE_ACCURACY_VALUE',
'Maximum model space distance between geometric entities at asserted c
onnectivities');
#74512=UNCERTAINTY_MEASURE_WITH_UNIT(LENGTH_MEASURE(0.01),#74524,
'DISTANCE_ACCURACY_VALUE',
'Maximum model space distance between geometric entities at asserted c
onnectivities');
#74522=(
GEOMETRIC_REPRESENTATION_CONTEXT(3)
GLOBAL_UNCERTAINTY_ASSIGNED_CONTEXT((#74511))
GLOBAL_UNIT_ASSIGNED_CONTEXT((#74524,#74526,#74527))
REPRESENTATION_CONTEXT('','3D')
);
#74523=(
GEOMETRIC_REPRESENTATION_CONTEXT(3)
GLOBAL_UNCERTAINTY_ASSIGNED_CONTEXT((#74512))
GLOBAL_UNIT_ASSIGNED_CONTEXT((#74524,#74526,#74527))
REPRESENTATION_CONTEXT('','3D')
);
#74524=(
LENGTH_UNIT()
NAMED_UNIT(*)
SI_UNIT(.MILLI.,.METRE.)
);
#74526=(
NAMED_UNIT(*)
PLANE_ANGLE_UNIT()
SI_UNIT($,.RADIAN.)
);
#74527=(
NAMED_UNIT(*)
SI_UNIT($,.STERADIAN.)
SOLID_ANGLE_UNIT()
);
#74537=SHAPE_DEFINITION_REPRESENTATION(#74547,#74566);
#74547=PRODUCT_DEFINITION_SHAPE('',$,#74577);
#74566=SHAPE_REPRESENTATION('',(#5069),#74522);
#74567=PRODUCT_DEFINITION_CONTEXT('part definition',#74599,'design');
#74577=PRODUCT_DEFINITION('Screw','Screw',#74587,#74567);
#74587=PRODUCT_DEFINITION_FORMATION('',$,#74610);
#74599=APPLICATION_CONTEXT(
'Core Data for Automotive Mechanical Design Process');
#74600=PRODUCT_CONTEXT('part definition',#74599,'mechanical');
#74610=PRODUCT('Screw','Screw',$,(#74600));
#74613=PRESENTATION_STYLE_ASSIGNMENT((#74616));
#74616=SURFACE_STYLE_USAGE(.BOTH.,#74619);
#74619=SURFACE_SIDE_STYLE('',(#74622));
#74622=SURFACE_STYLE_FILL_AREA(#74625);
#74625=FILL_AREA_STYLE('Opaque(255,255,255)',(#74628));
#74628=FILL_AREA_STYLE_COLOUR('Opaque(255,255,255)',#74631);
#74631=COLOUR_RGB('Opaque(255,255,255)', 0.31764706, 0.68627451, 0.89019608);
ENDSEC;
END-ISO-10303-21;
